ISO-10303-21;
HEADER;
/* Generated by software containing ST-Developer
 * from STEP Tools, Inc. (www.steptools.com) 
 */

FILE_DESCRIPTION(
/* description */ (''),
/* implementation_level */ '2;1');

FILE_NAME(
/* name */ 'Rod_01.step',
/* time_stamp */ '2026-10-05T14:32:37-07:00',
/* author */ (''),
/* organization */ (''),
/* preprocessor_version */ 'ST-DEVELOPER v20.2',
/* originating_system */ 'Autodesk Translation Framework v15.15.0.0',
/* authorisation */ '');

FILE_SCHEMA (('AUTOMOTIVE_DESIGN { 1 0 10303 214 3 1 1 }'));
ENDSEC;

DATA;
#10=MECHANICAL_DESIGN_GEOMETRIC_PRESENTATION_REPRESENTATION('',(#497),#74103);
#47=B_SPLINE_SURFACE_WITH_KNOTS('',3,3,((#69430,#69431,#69432,#69433,#69434,
#69435,#69436,#69437,#69438,#69439,#69440,#69441,#69442,#69443,#69444,#69445,
#69446,#69447,#69448,#69449,#69450,#69451,#69452,#69453,#69454,#69455,#69456,
#69457,#69458,#69459,#69460,#69461,#69462,#69463,#69464,#69465,#69466,#69467,
#69468,#69469,#69470,#69471,#69472,#69473,#69474,#69475,#69476,#69477,#69478,
#69479,#69480,#69481,#69482,#69483,#69484,#69485,#69486,#69487,#69488,#69489,
#69490,#69491,#69492,#69493,#69494,#69495,#69496,#69497,#69498,#69499,#69500,
#69501,#69502,#69503,#69504,#69505,#69506,#69507,#69508,#69509,#69510,#69511,
#69512,#69513,#69514,#69515,#69516,#69517,#69518,#69519,#69520,#69521,#69522,
#69523,#69524,#69525,#69526,#69527,#69528,#69529,#69530,#69531,#69532,#69533,
#69534,#69535,#69536,#69537,#69538,#69539,#69540,#69541,#69542,#69543,#69544,
#69545,#69546,#69547,#69548,#69549,#69550,#69551,#69552,#69553,#69554,#69555,
#69556,#69557,#69558,#69559,#69560,#69561,#69562,#69563,#69564,#69565,#69566,
#69567,#69568,#69569,#69570,#69571,#69572,#69573,#69574,#69575,#69576,#69577,
#69578,#69579,#69580,#69581,#69582,#69583,#69584,#69585,#69586,#69587,#69588,
#69589,#69590,#69591,#69592,#69593,#69594,#69595,#69596,#69597,#69598,#69599,
#69600,#69601,#69602,#69603,#69604,#69605,#69606,#69607,#69608,#69609,#69610,
#69611,#69612,#69613,#69614,#69615,#69616,#69617,#69618,#69619,#69620,#69621,
#69622,#69623,#69624,#69625,#69626,#69627,#69628,#69629,#69630,#69631,#69632,
#69633,#69634,#69635,#69636,#69637,#69638,#69639,#69640,#69641,#69642,#69643,
#69644,#69645,#69646,#69647,#69648,#69649,#69650,#69651,#69652,#69653,#69654,
#69655,#69656,#69657,#69658,#69659,#69660,#69661,#69662,#69663,#69664,#69665,
#69666,#69667,#69668,#69669,#69670,#69671,#69672,#69673,#69674,#69675,#69676,
#69677,#69678,#69679,#69680,#69681,#69682,#69683,#69684,#69685,#69686,#69687,
#69688,#69689,#69690,#69691,#69692,#69693,#69694,#69695,#69696,#69697,#69698,
#69699,#69700,#69701,#69702,#69703,#69704,#69705,#69706,#69707,#69708,#69709,
#69710,#69711,#69712,#69713,#69714,#69715,#69716,#69717,#69718,#69719,#69720,
#69721,#69722,#69723,#69724,#69725,#69726,#69727,#69728,#69729,#69730,#69731,
#69732,#69733,#69734,#69735,#69736,#69737,#69738,#69739,#69740,#69741,#69742,
#69743,#69744,#69745,#69746,#69747,#69748,#69749,#69750,#69751,#69752,#69753,
#69754,#69755,#69756,#69757,#69758,#69759,#69760,#69761,#69762,#69763,#69764,
#69765,#69766,#69767,#69768,#69769,#69770,#69771,#69772,#69773,#69774,#69775,
#69776,#69777,#69778,#69779,#69780,#69781,#69782,#69783,#69784,#69785,#69786,
#69787,#69788,#69789,#69790,#69791,#69792,#69793,#69794,#69795,#69796,#69797,
#69798,#69799,#69800,#69801,#69802,#69803,#69804,#69805,#69806,#69807,#69808,
#69809,#69810,#69811,#69812,#69813,#69814,#69815,#69816,#69817,#69818,#69819,
#69820,#69821,#69822,#69823,#69824,#69825,#69826,#69827,#69828,#69829,#69830,
#69831,#69832,#69833,#69834,#69835,#69836,#69837,#69838,#69839,#69840,#69841,
#69842,#69843,#69844,#69845,#69846,#69847,#69848,#69849,#69850,#69851,#69852,
#69853,#69854,#69855,#69856,#69857,#69858,#69859,#69860,#69861,#69862,#69863,
#69864,#69865,#69866,#69867,#69868,#69869,#69870,#69871,#69872,#69873,#69874,
#69875,#69876,#69877,#69878,#69879,#69880,#69881,#69882,#69883,#69884,#69885,
#69886,#69887,#69888,#69889,#69890,#69891,#69892,#69893,#69894,#69895,#69896,
#69897,#69898,#69899,#69900,#69901,#69902,#69903,#69904,#69905,#69906,#69907,
#69908,#69909,#69910,#69911,#69912,#69913,#69914,#69915,#69916,#69917,#69918,
#69919,#69920,#69921,#69922,#69923,#69924,#69925,#69926,#69927,#69928,#69929,
#69930,#69931,#69932,#69933,#69934,#69935,#69936,#69937,#69938,#69939,#69940,
#69941,#69942,#69943,#69944,#69945,#69946,#69947,#69948,#69949,#69950,#69951,
#69952,#69953,#69954,#69955,#69956,#69957,#69958,#69959,#69960,#69961,#69962),
(#69963,#69964,#69965,#69966,#69967,#69968,#69969,#69970,#69971,#69972,
#69973,#69974,#69975,#69976,#69977,#69978,#69979,#69980,#69981,#69982,#69983,
#69984,#69985,#69986,#69987,#69988,#69989,#69990,#69991,#69992,#69993,#69994,
#69995,#69996,#69997,#69998,#69999,#70000,#70001,#70002,#70003,#70004,#70005,
#70006,#70007,#70008,#70009,#70010,#70011,#70012,#70013,#70014,#70015,#70016,
#70017,#70018,#70019,#70020,#70021,#70022,#70023,#70024,#70025,#70026,#70027,
#70028,#70029,#70030,#70031,#70032,#70033,#70034,#70035,#70036,#70037,#70038,
#70039,#70040,#70041,#70042,#70043,#70044,#70045,#70046,#70047,#70048,#70049,
#70050,#70051,#70052,#70053,#70054,#70055,#70056,#70057,#70058,#70059,#70060,
#70061,#70062,#70063,#70064,#70065,#70066,#70067,#70068,#70069,#70070,#70071,
#70072,#70073,#70074,#70075,#70076,#70077,#70078,#70079,#70080,#70081,#70082,
#70083,#70084,#70085,#70086,#70087,#70088,#70089,#70090,#70091,#70092,#70093,
#70094,#70095,#70096,#70097,#70098,#70099,#70100,#70101,#70102,#70103,#70104,
#70105,#70106,#70107,#70108,#70109,#70110,#70111,#70112,#70113,#70114,#70115,
#70116,#70117,#70118,#70119,#70120,#70121,#70122,#70123,#70124,#70125,#70126,
#70127,#70128,#70129,#70130,#70131,#70132,#70133,#70134,#70135,#70136,#70137,
#70138,#70139,#70140,#70141,#70142,#70143,#70144,#70145,#70146,#70147,#70148,
#70149,#70150,#70151,#70152,#70153,#70154,#70155,#70156,#70157,#70158,#70159,
#70160,#70161,#70162,#70163,#70164,#70165,#70166,#70167,#70168,#70169,#70170,
#70171,#70172,#70173,#70174,#70175,#70176,#70177,#70178,#70179,#70180,#70181,
#70182,#70183,#70184,#70185,#70186,#70187,#70188,#70189,#70190,#70191,#70192,
#70193,#70194,#70195,#70196,#70197,#70198,#70199,#70200,#70201,#70202,#70203,
#70204,#70205,#70206,#70207,#70208,#70209,#70210,#70211,#70212,#70213,#70214,
#70215,#70216,#70217,#70218,#70219,#70220,#70221,#70222,#70223,#70224,#70225,
#70226,#70227,#70228,#70229,#70230,#70231,#70232,#70233,#70234,#70235,#70236,
#70237,#70238,#70239,#70240,#70241,#70242,#70243,#70244,#70245,#70246,#70247,
#70248,#70249,#70250,#70251,#70252,#70253,#70254,#70255,#70256,#70257,#70258,
#70259,#70260,#70261,#70262,#70263,#70264,#70265,#70266,#70267,#70268,#70269,
#70270,#70271,#70272,#70273,#70274,#70275,#70276,#70277,#70278,#70279,#70280,
#70281,#70282,#70283,#70284,#70285,#70286,#70287,#70288,#70289,#70290,#70291,
#70292,#70293,#70294,#70295,#70296,#70297,#70298,#70299,#70300,#70301,#70302,
#70303,#70304,#70305,#70306,#70307,#70308,#70309,#70310,#70311,#70312,#70313,
#70314,#70315,#70316,#70317,#70318,#70319,#70320,#70321,#70322,#70323,#70324,
#70325,#70326,#70327,#70328,#70329,#70330,#70331,#70332,#70333,#70334,#70335,
#70336,#70337,#70338,#70339,#70340,#70341,#70342,#70343,#70344,#70345,#70346,
#70347,#70348,#70349,#70350,#70351,#70352,#70353,#70354,#70355,#70356,#70357,
#70358,#70359,#70360,#70361,#70362,#70363,#70364,#70365,#70366,#70367,#70368,
#70369,#70370,#70371,#70372,#70373,#70374,#70375,#70376,#70377,#70378,#70379,
#70380,#70381,#70382,#70383,#70384,#70385,#70386,#70387,#70388,#70389,#70390,
#70391,#70392,#70393,#70394,#70395,#70396,#70397,#70398,#70399,#70400,#70401,
#70402,#70403,#70404,#70405,#70406,#70407,#70408,#70409,#70410,#70411,#70412,
#70413,#70414,#70415,#70416,#70417,#70418,#70419,#70420,#70421,#70422,#70423,
#70424,#70425,#70426,#70427,#70428,#70429,#70430,#70431,#70432,#70433,#70434,
#70435,#70436,#70437,#70438,#70439,#70440,#70441,#70442,#70443,#70444,#70445,
#70446,#70447,#70448,#70449,#70450,#70451,#70452,#70453,#70454,#70455,#70456,
#70457,#70458,#70459,#70460,#70461,#70462,#70463,#70464,#70465,#70466,#70467,
#70468,#70469,#70470,#70471,#70472,#70473,#70474,#70475,#70476,#70477,#70478,
#70479,#70480,#70481,#70482,#70483,#70484,#70485,#70486,#70487,#70488,#70489,
#70490,#70491,#70492,#70493,#70494,#70495),(#70496,#70497,#70498,#70499,
#70500,#70501,#70502,#70503,#70504,#70505,#70506,#70507,#70508,#70509,#70510,
#70511,#70512,#70513,#70514,#70515,#70516,#70517,#70518,#70519,#70520,#70521,
#70522,#70523,#70524,#70525,#70526,#70527,#70528,#70529,#70530,#70531,#70532,
#70533,#70534,#70535,#70536,#70537,#70538,#70539,#70540,#70541,#70542,#70543,
#70544,#70545,#70546,#70547,#70548,#70549,#70550,#70551,#70552,#70553,#70554,
#70555,#70556,#70557,#70558,#70559,#70560,#70561,#70562,#70563,#70564,#70565,
#70566,#70567,#70568,#70569,#70570,#70571,#70572,#70573,#70574,#70575,#70576,
#70577,#70578,#70579,#70580,#70581,#70582,#70583,#70584,#70585,#70586,#70587,
#70588,#70589,#70590,#70591,#70592,#70593,#70594,#70595,#70596,#70597,#70598,
#70599,#70600,#70601,#70602,#70603,#70604,#70605,#70606,#70607,#70608,#70609,
#70610,#70611,#70612,#70613,#70614,#70615,#70616,#70617,#70618,#70619,#70620,
#70621,#70622,#70623,#70624,#70625,#70626,#70627,#70628,#70629,#70630,#70631,
#70632,#70633,#70634,#70635,#70636,#70637,#70638,#70639,#70640,#70641,#70642,
#70643,#70644,#70645,#70646,#70647,#70648,#70649,#70650,#70651,#70652,#70653,
#70654,#70655,#70656,#70657,#70658,#70659,#70660,#70661,#70662,#70663,#70664,
#70665,#70666,#70667,#70668,#70669,#70670,#70671,#70672,#70673,#70674,#70675,
#70676,#70677,#70678,#70679,#70680,#70681,#70682,#70683,#70684,#70685,#70686,
#70687,#70688,#70689,#70690,#70691,#70692,#70693,#70694,#70695,#70696,#70697,
#70698,#70699,#70700,#70701,#70702,#70703,#70704,#70705,#70706,#70707,#70708,
#70709,#70710,#70711,#70712,#70713,#70714,#70715,#70716,#70717,#70718,#70719,
#70720,#70721,#70722,#70723,#70724,#70725,#70726,#70727,#70728,#70729,#70730,
#70731,#70732,#70733,#70734,#70735,#70736,#70737,#70738,#70739,#70740,#70741,
#70742,#70743,#70744,#70745,#70746,#70747,#70748,#70749,#70750,#70751,#70752,
#70753,#70754,#70755,#70756,#70757,#70758,#70759,#70760,#70761,#70762,#70763,
#70764,#70765,#70766,#70767,#70768,#70769,#70770,#70771,#70772,#70773,#70774,
#70775,#70776,#70777,#70778,#70779,#70780,#70781,#70782,#70783,#70784,#70785,
#70786,#70787,#70788,#70789,#70790,#70791,#70792,#70793,#70794,#70795,#70796,
#70797,#70798,#70799,#70800,#70801,#70802,#70803,#70804,#70805,#70806,#70807,
#70808,#70809,#70810,#70811,#70812,#70813,#70814,#70815,#70816,#70817,#70818,
#70819,#70820,#70821,#70822,#70823,#70824,#70825,#70826,#70827,#70828,#70829,
#70830,#70831,#70832,#70833,#70834,#70835,#70836,#70837,#70838,#70839,#70840,
#70841,#70842,#70843,#70844,#70845,#70846,#70847,#70848,#70849,#70850,#70851,
#70852,#70853,#70854,#70855,#70856,#70857,#70858,#70859,#70860,#70861,#70862,
#70863,#70864,#70865,#70866,#70867,#70868,#70869,#70870,#70871,#70872,#70873,
#70874,#70875,#70876,#70877,#70878,#70879,#70880,#70881,#70882,#70883,#70884,
#70885,#70886,#70887,#70888,#70889,#70890,#70891,#70892,#70893,#70894,#70895,
#70896,#70897,#70898,#70899,#70900,#70901,#70902,#70903,#70904,#70905,#70906,
#70907,#70908,#70909,#70910,#70911,#70912,#70913,#70914,#70915,#70916,#70917,
#70918,#70919,#70920,#70921,#70922,#70923,#70924,#70925,#70926,#70927,#70928,
#70929,#70930,#70931,#70932,#70933,#70934,#70935,#70936,#70937,#70938,#70939,
#70940,#70941,#70942,#70943,#70944,#70945,#70946,#70947,#70948,#70949,#70950,
#70951,#70952,#70953,#70954,#70955,#70956,#70957,#70958,#70959,#70960,#70961,
#70962,#70963,#70964,#70965,#70966,#70967,#70968,#70969,#70970,#70971,#70972,
#70973,#70974,#70975,#70976,#70977,#70978,#70979,#70980,#70981,#70982,#70983,
#70984,#70985,#70986,#70987,#70988,#70989,#70990,#70991,#70992,#70993,#70994,
#70995,#70996,#70997,#70998,#70999,#71000,#71001,#71002,#71003,#71004,#71005,
#71006,#71007,#71008,#71009,#71010,#71011,#71012,#71013,#71014,#71015,#71016,
#71017,#71018,#71019,#71020,#71021,#71022,#71023,#71024,#71025,#71026,#71027,
#71028),(#71029,#71030,#71031,#71032,#71033,#71034,#71035,#71036,#71037,
#71038,#71039,#71040,#71041,#71042,#71043,#71044,#71045,#71046,#71047,#71048,
#71049,#71050,#71051,#71052,#71053,#71054,#71055,#71056,#71057,#71058,#71059,
#71060,#71061,#71062,#71063,#71064,#71065,#71066,#71067,#71068,#71069,#71070,
#71071,#71072,#71073,#71074,#71075,#71076,#71077,#71078,#71079,#71080,#71081,
#71082,#71083,#71084,#71085,#71086,#71087,#71088,#71089,#71090,#71091,#71092,
#71093,#71094,#71095,#71096,#71097,#71098,#71099,#71100,#71101,#71102,#71103,
#71104,#71105,#71106,#71107,#71108,#71109,#71110,#71111,#71112,#71113,#71114,
#71115,#71116,#71117,#71118,#71119,#71120,#71121,#71122,#71123,#71124,#71125,
#71126,#71127,#71128,#71129,#71130,#71131,#71132,#71133,#71134,#71135,#71136,
#71137,#71138,#71139,#71140,#71141,#71142,#71143,#71144,#71145,#71146,#71147,
#71148,#71149,#71150,#71151,#71152,#71153,#71154,#71155,#71156,#71157,#71158,
#71159,#71160,#71161,#71162,#71163,#71164,#71165,#71166,#71167,#71168,#71169,
#71170,#71171,#71172,#71173,#71174,#71175,#71176,#71177,#71178,#71179,#71180,
#71181,#71182,#71183,#71184,#71185,#71186,#71187,#71188,#71189,#71190,#71191,
#71192,#71193,#71194,#71195,#71196,#71197,#71198,#71199,#71200,#71201,#71202,
#71203,#71204,#71205,#71206,#71207,#71208,#71209,#71210,#71211,#71212,#71213,
#71214,#71215,#71216,#71217,#71218,#71219,#71220,#71221,#71222,#71223,#71224,
#71225,#71226,#71227,#71228,#71229,#71230,#71231,#71232,#71233,#71234,#71235,
#71236,#71237,#71238,#71239,#71240,#71241,#71242,#71243,#71244,#71245,#71246,
#71247,#71248,#71249,#71250,#71251,#71252,#71253,#71254,#71255,#71256,#71257,
#71258,#71259,#71260,#71261,#71262,#71263,#71264,#71265,#71266,#71267,#71268,
#71269,#71270,#71271,#71272,#71273,#71274,#71275,#71276,#71277,#71278,#71279,
#71280,#71281,#71282,#71283,#71284,#71285,#71286,#71287,#71288,#71289,#71290,
#71291,#71292,#71293,#71294,#71295,#71296,#71297,#71298,#71299,#71300,#71301,
#71302,#71303,#71304,#71305,#71306,#71307,#71308,#71309,#71310,#71311,#71312,
#71313,#71314,#71315,#71316,#71317,#71318,#71319,#71320,#71321,#71322,#71323,
#71324,#71325,#71326,#71327,#71328,#71329,#71330,#71331,#71332,#71333,#71334,
#71335,#71336,#71337,#71338,#71339,#71340,#71341,#71342,#71343,#71344,#71345,
#71346,#71347,#71348,#71349,#71350,#71351,#71352,#71353,#71354,#71355,#71356,
#71357,#71358,#71359,#71360,#71361,#71362,#71363,#71364,#71365,#71366,#71367,
#71368,#71369,#71370,#71371,#71372,#71373,#71374,#71375,#71376,#71377,#71378,
#71379,#71380,#71381,#71382,#71383,#71384,#71385,#71386,#71387,#71388,#71389,
#71390,#71391,#71392,#71393,#71394,#71395,#71396,#71397,#71398,#71399,#71400,
#71401,#71402,#71403,#71404,#71405,#71406,#71407,#71408,#71409,#71410,#71411,
#71412,#71413,#71414,#71415,#71416,#71417,#71418,#71419,#71420,#71421,#71422,
#71423,#71424,#71425,#71426,#71427,#71428,#71429,#71430,#71431,#71432,#71433,
#71434,#71435,#71436,#71437,#71438,#71439,#71440,#71441,#71442,#71443,#71444,
#71445,#71446,#71447,#71448,#71449,#71450,#71451,#71452,#71453,#71454,#71455,
#71456,#71457,#71458,#71459,#71460,#71461,#71462,#71463,#71464,#71465,#71466,
#71467,#71468,#71469,#71470,#71471,#71472,#71473,#71474,#71475,#71476,#71477,
#71478,#71479,#71480,#71481,#71482,#71483,#71484,#71485,#71486,#71487,#71488,
#71489,#71490,#71491,#71492,#71493,#71494,#71495,#71496,#71497,#71498,#71499,
#71500,#71501,#71502,#71503,#71504,#71505,#71506,#71507,#71508,#71509,#71510,
#71511,#71512,#71513,#71514,#71515,#71516,#71517,#71518,#71519,#71520,#71521,
#71522,#71523,#71524,#71525,#71526,#71527,#71528,#71529,#71530,#71531,#71532,
#71533,#71534,#71535,#71536,#71537,#71538,#71539,#71540,#71541,#71542,#71543,
#71544,#71545,#71546,#71547,#71548,#71549,#71550,#71551,#71552,#71553,#71554,
#71555,#71556,#71557,#71558,#71559,#71560,#71561)),.UNSPECIFIED.,.F.,.F.,
 .F.,(4,4),(4,1,1,1,1,1,1,1,1,1,1,1,1,1,1,1,1,1,1,1,1,1,1,1,1,1,1,1,1,1,
1,1,1,1,1,1,1,1,1,1,1,1,1,1,1,1,1,1,1,1,1,1,1,1,1,1,1,1,1,1,1,1,1,1,1,1,
1,1,1,1,1,1,1,1,1,1,1,1,1,1,1,1,1,1,1,1,1,1,1,1,1,1,1,1,1,1,1,1,1,1,1,1,
1,1,1,1,1,1,1,1,1,1,1,1,1,1,1,1,1,1,1,1,1,1,1,1,1,1,1,1,1,1,1,1,1,1,1,1,
1,1,1,1,1,1,1,1,1,1,1,1,1,1,1,1,1,1,1,1,1,1,1,1,1,1,1,1,1,1,1,1,1,1,1,1,
1,1,1,1,1,1,1,1,1,1,1,1,1,1,1,1,1,1,1,1,1,1,1,1,1,1,1,1,1,1,1,1,1,1,1,1,
1,1,1,1,1,1,1,1,1,1,1,1,1,1,1,1,1,1,1,1,1,1,1,1,1,1,1,1,1,1,1,1,1,1,1,1,
1,1,1,1,1,1,1,1,1,1,1,1,1,1,1,1,1,1,1,1,1,1,1,1,1,1,1,1,1,1,1,1,1,1,1,1,
1,1,1,1,1,1,1,1,1,1,1,1,1,1,1,1,1,1,1,1,1,1,1,1,1,1,1,1,1,1,1,1,1,1,1,1,
1,1,1,1,1,1,1,1,1,1,1,1,1,1,1,1,1,1,1,1,1,1,1,1,1,1,1,1,1,1,1,1,1,1,1,1,
1,1,1,1,1,1,1,1,1,1,1,1,1,1,1,1,1,1,1,1,1,1,1,1,1,1,1,1,1,1,1,1,1,1,1,1,
1,1,1,1,1,1,1,1,1,1,1,1,1,1,1,1,1,1,1,1,1,1,1,1,1,1,1,1,1,1,1,1,1,1,1,1,
1,1,1,1,1,1,1,1,1,1,1,1,1,1,1,1,1,1,1,1,1,1,1,1,1,1,1,1,1,1,1,1,1,1,1,1,
1,1,1,1,1,1,1,1,1,1,1,1,1,1,1,1,1,1,1,1,1,1,1,1,1,1,1,1,1,1,1,1,1,1,1,1,
1,1,1,1,1,1,1,1,1,1,1,1,1,1,1,1,1,1,1,1,1,1,1,1,1,1,1,1,1,1,1,1,4),(-0.000646701964609084,
0.0823585128613958),(8.31473274985906,9.3144474053319,10.3141620608047,
11.3138767162776,12.3135913717504,13.3133060272232,14.3130206826961,15.3127353381689,
16.3124499936417,17.3121646491146,18.3118793045874,19.3115939600602,20.3113086155331,
21.3110232710059,22.3107379264787,23.3104525819516,24.3101672374244,25.3098818928972,
26.30959654837,27.3093112038429,28.3090258593157,29.3087405147885,30.3084551702614,
31.3081698257342,32.307884481207,33.3075991366799,34.3073137921527,35.3070284476255,
36.3067431030984,37.3064577585712,38.306172414044,39.3058870695169,40.3056017249897,
41.3053163804625,42.3050310359354,43.3047456914082,44.304460346881,45.3041750023539,
46.3038896578267,47.3036043132995,48.3033189687724,49.3030336242452,50.302748279718,
51.3024629351909,52.3021775906637,53.3018922461365,54.3016069016094,55.3013215570822,
56.301036212555,57.3007508680278,58.3004655235007,59.3001801789735,60.2998948344463,
61.2996094899192,62.299324145392,63.2990388008648,64.2987534563377,65.2984681118105,
66.2981827672834,67.2978974227562,68.297612078229,69.2973267337018,70.2970413891747,
71.2967560446475,72.2964707001203,73.2961853555932,74.295900011066,75.2956146665388,
76.2953293220117,77.2950439774845,78.2947586329573,79.2944732884302,80.294187943903,
81.2939025993758,82.2936172548487,83.2933319103215,84.2930465657943,85.2927612212672,
86.29247587674,87.2921905322128,88.2919051876857,89.2916198431585,90.2913344986313,
91.2910491541042,92.290763809577,93.2904784650498,94.2901931205227,95.2899077759955,
96.2896224314683,97.2893370869411,98.289051742414,99.2887663978868,100.28848105336,
101.288195708832,102.287910364305,103.287625019778,104.287339675251,105.287054330724,
106.286768986197,107.286483641669,108.286198297142,109.285912952615,110.285627608088,
111.285342263561,112.285056919034,113.284771574506,114.284486229979,115.284200885452,
116.283915540925,117.283630196398,118.283344851871,119.283059507343,120.282774162816,
121.282488818289,122.282203473762,123.281918129235,124.281632784708,125.28134744018,
126.281062095653,127.280776751126,128.280491406599,129.280206062072,130.279920717545,
131.279635373017,132.27935002849,133.279064683963,134.278779339436,135.278493994909,
136.278208650382,137.277923305854,138.277637961327,139.2773526168,140.277067272273,
141.276781927746,142.276496583219,143.276211238691,144.275925894164,145.275640549637,
146.27535520511,147.275069860583,148.274784516056,149.274499171528,150.274213827001,
151.273928482474,152.273643137947,153.27335779342,154.273072448893,155.272787104365,
156.272501759838,157.272216415311,158.271931070784,159.271645726257,160.27136038173,
161.271075037202,162.270789692675,163.270504348148,164.270219003621,165.269933659094,
166.269648314567,167.269362970039,168.269077625512,169.268792280985,170.268506936458,
171.268221591931,172.267936247404,173.267650902876,174.267365558349,175.267080213822,
176.266794869295,177.266509524768,178.266224180241,179.265938835713,180.265653491186,
181.265368146659,182.265082802132,183.264797457605,184.264512113078,185.26422676855,
186.263941424023,187.263656079496,188.263370734969,189.263085390442,190.262800045915,
191.262514701387,192.26222935686,193.261944012333,194.261658667806,195.261373323279,
196.261087978752,197.260802634224,198.260517289697,199.26023194517,200.259946600643,
201.259661256116,202.259375911589,203.259090567061,204.258805222534,205.258519878007,
206.25823453348,207.257949188953,208.257663844426,209.257378499898,210.257093155371,
211.256807810844,212.256522466317,213.25623712179,214.255951777263,215.255666432735,
216.255381088208,217.255095743681,218.254810399154,219.254525054627,220.2542397101,
221.253954365572,222.253669021045,223.253383676518,224.253098331991,225.252812987464,
226.252527642937,227.252242298409,228.251956953882,229.251671609355,230.251386264828,
231.251100920301,232.250815575774,233.250530231246,234.250244886719,235.249959542192,
236.249674197665,237.249388853138,238.249103508611,239.248818164083,240.248532819556,
241.248247475029,242.247962130502,243.247676785975,244.247391441448,245.24710609692,
246.246820752393,247.246535407866,248.246250063339,249.245964718812,250.245679374285,
251.245394029757,252.24510868523,253.244823340703,254.244537996176,255.244252651649,
256.243967307122,257.243681962594,258.243396618067,259.24311127354,260.242825929013,
261.242540584486,262.242255239959,263.241969895431,264.241684550904,265.241399206377,
266.24111386185,267.240828517323,268.240543172795,269.240257828268,270.239972483741,
271.239687139214,272.239401794687,273.23911645016,274.238831105632,275.238545761105,
276.238260416578,277.237975072051,278.237689727524,279.237404382997,280.237119038469,
281.236833693942,282.236548349415,283.236263004888,284.235977660361,285.235692315834,
286.235406971306,287.235121626779,288.234836282252,289.234550937725,290.234265593198,
291.233980248671,292.233694904143,293.233409559616,294.233124215089,295.232838870562,
296.232553526035,297.232268181508,298.23198283698,299.231697492453,300.231412147926,
301.231126803399,302.230841458872,303.230556114345,304.230270769817,305.22998542529,
306.229700080763,307.229414736236,308.229129391709,309.228844047182,310.228558702654,
311.228273358127,312.2279880136,313.227702669073,314.227417324546,315.227131980019,
316.226846635491,317.226561290964,318.226275946437,319.22599060191,320.225705257383,
321.225419912856,322.225134568328,323.224849223801,324.224563879274,325.224278534747,
326.22399319022,327.223707845693,328.223422501165,329.223137156638,330.222851812111,
331.222566467584,332.222281123057,333.22199577853,334.221710434002,335.221425089475,
336.221139744948,337.220854400421,338.220569055894,339.220283711367,340.219998366839,
341.219713022312,342.219427677785,343.219142333258,344.218856988731,345.218571644204,
346.218286299676,347.218000955149,348.217715610622,349.217430266095,350.217144921568,
351.216859577041,352.216574232513,353.216288887986,354.216003543459,355.215718198932,
356.215432854405,357.215147509878,358.21486216535,359.214576820823,360.214291476296,
361.214006131769,362.213720787242,363.213435442715,364.213150098187,365.21286475366,
366.212579409133,367.212294064606,368.212008720079,369.211723375552,370.211438031024,
371.211152686497,372.21086734197,373.210581997443,374.210296652916,375.210011308389,
376.209725963861,377.209440619334,378.209155274807,379.20886993028,380.208584585753,
381.208299241226,382.208013896698,383.207728552171,384.207443207644,385.207157863117,
386.20687251859,387.206587174063,388.206301829535,389.206016485008,390.205731140481,
391.205445795954,392.205160451427,393.2048751069,394.204589762372,395.204304417845,
396.204019073318,397.203733728791,398.203448384264,399.203163039737,400.202877695209,
401.202592350682,402.202307006155,403.202021661628,404.201736317101,405.201450972574,
406.201165628046,407.200880283519,408.200594938992,409.200309594465,410.200024249938,
411.199738905411,412.199453560883,413.199168216356,414.198882871829,415.198597527302,
416.198312182775,417.198026838248,418.19774149372,419.197456149193,420.197170804666,
421.196885460139,422.196600115612,423.196314771085,424.196029426557,425.19574408203,
426.195458737503,427.195173392976,428.194888048449,429.194602703922,430.194317359394,
431.194032014867,432.19374667034,433.193461325813,434.193175981286,435.192890636758,
436.192605292231,437.192319947704,438.192034603177,439.19174925865,440.191463914123,
441.191178569595,442.190893225068,443.190607880541,444.190322536014,445.190037191487,
446.18975184696,447.189466502432,448.189181157905,449.188895813378,450.188610468851,
451.188325124324,452.188039779797,453.187754435269,454.187469090742,455.187183746215,
456.186898401688,457.186613057161,458.186327712634,459.186042368106,460.185757023579,
461.185471679052,462.185186334525,463.184900989998,464.184615645471,465.184330300943,
466.184044956416,467.183759611889,468.183474267362,469.183188922835,470.182903578308,
471.18261823378,472.182332889253,473.182047544726,474.181762200199,475.181476855672,
476.181191511145,477.180906166617,478.18062082209,479.180335477563,480.180050133036,
481.179764788509,482.179479443982,483.179194099454,484.178908754927,485.1786234104,
486.178338065873,487.178052721346,488.177767376819,489.177482032291,490.177196687764,
491.176911343237,492.17662599871,493.176340654183,494.176055309656,495.175769965128,
496.175484620601,497.175199276074,498.174913931547,499.17462858702,500.174343242493,
501.174057897965,502.173772553438,503.173487208911,504.173201864384,505.172916519857,
506.17263117533,507.172345830802,508.172060486275,509.171775141748,510.171489797221,
511.171204452694,512.170919108167,513.170633763639,514.170348419112,515.170063074585,
516.169777730058,517.169492385531,518.169207041004,519.168921696476,520.168636351949,
521.168351007422,522.168065662895,523.167780318368,524.167494973841,525.167209629313,
526.166924284786,527.166638940259,528.166353595732,529.166068251205,530.165782906678,
531.16549756215,532.165212217623,533.164926873096,534.164641528569,535.164356184042,
536.164070839515,537.163785494987,538.164146852425),.UNSPECIFIED.);
#48=B_SPLINE_SURFACE_WITH_KNOTS('',3,3,((#71753,#71754,#71755,#71756,#71757,
#71758,#71759,#71760,#71761,#71762,#71763,#71764,#71765,#71766,#71767,#71768,
#71769,#71770,#71771,#71772,#71773,#71774,#71775,#71776,#71777,#71778,#71779,
#71780,#71781,#71782,#71783,#71784,#71785,#71786,#71787,#71788,#71789,#71790,
#71791,#71792,#71793,#71794,#71795,#71796,#71797,#71798,#71799,#71800,#71801,
#71802,#71803,#71804,#71805,#71806,#71807,#71808,#71809,#71810,#71811,#71812,
#71813,#71814,#71815,#71816,#71817,#71818,#71819,#71820,#71821,#71822,#71823,
#71824,#71825,#71826,#71827,#71828,#71829,#71830,#71831,#71832,#71833,#71834,
#71835,#71836,#71837,#71838,#71839,#71840,#71841,#71842,#71843,#71844,#71845,
#71846,#71847,#71848,#71849,#71850,#71851,#71852,#71853,#71854,#71855,#71856,
#71857,#71858,#71859,#71860,#71861,#71862,#71863,#71864,#71865,#71866,#71867,
#71868,#71869,#71870,#71871,#71872,#71873,#71874,#71875,#71876,#71877,#71878,
#71879,#71880,#71881,#71882,#71883,#71884,#71885,#71886,#71887,#71888,#71889,
#71890,#71891,#71892,#71893,#71894,#71895,#71896,#71897,#71898,#71899,#71900,
#71901,#71902,#71903,#71904,#71905,#71906,#71907,#71908,#71909,#71910,#71911,
#71912,#71913,#71914,#71915,#71916,#71917,#71918,#71919,#71920,#71921,#71922,
#71923,#71924,#71925,#71926,#71927,#71928,#71929,#71930,#71931,#71932,#71933,
#71934,#71935,#71936,#71937,#71938,#71939,#71940,#71941,#71942,#71943,#71944,
#71945,#71946,#71947,#71948,#71949,#71950,#71951,#71952,#71953,#71954,#71955,
#71956,#71957,#71958,#71959,#71960,#71961,#71962,#71963,#71964,#71965,#71966,
#71967,#71968,#71969,#71970,#71971,#71972,#71973,#71974,#71975,#71976,#71977,
#71978,#71979,#71980,#71981,#71982,#71983,#71984,#71985,#71986,#71987,#71988,
#71989,#71990,#71991,#71992,#71993,#71994,#71995,#71996,#71997,#71998,#71999,
#72000,#72001,#72002,#72003,#72004,#72005,#72006,#72007,#72008,#72009,#72010,
#72011,#72012,#72013,#72014,#72015,#72016,#72017,#72018,#72019,#72020,#72021,
#72022,#72023,#72024,#72025,#72026,#72027,#72028,#72029,#72030,#72031,#72032,
#72033,#72034,#72035,#72036,#72037,#72038,#72039,#72040,#72041,#72042,#72043,
#72044,#72045,#72046,#72047,#72048,#72049,#72050,#72051,#72052,#72053,#72054,
#72055,#72056,#72057,#72058,#72059,#72060,#72061,#72062,#72063,#72064,#72065,
#72066,#72067,#72068,#72069,#72070,#72071,#72072,#72073,#72074,#72075,#72076,
#72077,#72078,#72079,#72080,#72081,#72082,#72083,#72084,#72085,#72086,#72087,
#72088,#72089,#72090,#72091,#72092,#72093,#72094,#72095,#72096,#72097,#72098,
#72099,#72100,#72101,#72102,#72103,#72104,#72105,#72106,#72107,#72108,#72109,
#72110,#72111,#72112,#72113,#72114,#72115,#72116,#72117,#72118,#72119,#72120,
#72121,#72122,#72123,#72124,#72125,#72126,#72127,#72128,#72129,#72130,#72131,
#72132,#72133,#72134,#72135,#72136,#72137,#72138,#72139,#72140,#72141,#72142,
#72143,#72144,#72145,#72146,#72147,#72148,#72149,#72150,#72151,#72152,#72153,
#72154,#72155,#72156,#72157,#72158,#72159,#72160,#72161,#72162,#72163,#72164,
#72165,#72166,#72167,#72168,#72169,#72170,#72171,#72172,#72173,#72174,#72175,
#72176,#72177,#72178,#72179,#72180,#72181,#72182,#72183,#72184,#72185,#72186,
#72187,#72188,#72189,#72190,#72191,#72192,#72193,#72194,#72195,#72196,#72197,
#72198,#72199,#72200,#72201,#72202,#72203,#72204,#72205,#72206,#72207,#72208,
#72209,#72210,#72211,#72212,#72213,#72214,#72215,#72216,#72217,#72218,#72219,
#72220,#72221,#72222,#72223,#72224,#72225,#72226,#72227,#72228,#72229,#72230,
#72231,#72232,#72233,#72234,#72235,#72236,#72237,#72238,#72239,#72240,#72241,
#72242,#72243,#72244,#72245,#72246,#72247,#72248,#72249,#72250,#72251,#72252,
#72253,#72254,#72255,#72256,#72257,#72258,#72259,#72260,#72261,#72262,#72263,
#72264,#72265,#72266,#72267,#72268,#72269,#72270,#72271,#72272,#72273,#72274,
#72275,#72276,#72277,#72278,#72279,#72280,#72281,#72282,#72283,#72284,#72285),
(#72286,#72287,#72288,#72289,#72290,#72291,#72292,#72293,#72294,#72295,
#72296,#72297,#72298,#72299,#72300,#72301,#72302,#72303,#72304,#72305,#72306,
#72307,#72308,#72309,#72310,#72311,#72312,#72313,#72314,#72315,#72316,#72317,
#72318,#72319,#72320,#72321,#72322,#72323,#72324,#72325,#72326,#72327,#72328,
#72329,#72330,#72331,#72332,#72333,#72334,#72335,#72336,#72337,#72338,#72339,
#72340,#72341,#72342,#72343,#72344,#72345,#72346,#72347,#72348,#72349,#72350,
#72351,#72352,#72353,#72354,#72355,#72356,#72357,#72358,#72359,#72360,#72361,
#72362,#72363,#72364,#72365,#72366,#72367,#72368,#72369,#72370,#72371,#72372,
#72373,#72374,#72375,#72376,#72377,#72378,#72379,#72380,#72381,#72382,#72383,
#72384,#72385,#72386,#72387,#72388,#72389,#72390,#72391,#72392,#72393,#72394,
#72395,#72396,#72397,#72398,#72399,#72400,#72401,#72402,#72403,#72404,#72405,
#72406,#72407,#72408,#72409,#72410,#72411,#72412,#72413,#72414,#72415,#72416,
#72417,#72418,#72419,#72420,#72421,#72422,#72423,#72424,#72425,#72426,#72427,
#72428,#72429,#72430,#72431,#72432,#72433,#72434,#72435,#72436,#72437,#72438,
#72439,#72440,#72441,#72442,#72443,#72444,#72445,#72446,#72447,#72448,#72449,
#72450,#72451,#72452,#72453,#72454,#72455,#72456,#72457,#72458,#72459,#72460,
#72461,#72462,#72463,#72464,#72465,#72466,#72467,#72468,#72469,#72470,#72471,
#72472,#72473,#72474,#72475,#72476,#72477,#72478,#72479,#72480,#72481,#72482,
#72483,#72484,#72485,#72486,#72487,#72488,#72489,#72490,#72491,#72492,#72493,
#72494,#72495,#72496,#72497,#72498,#72499,#72500,#72501,#72502,#72503,#72504,
#72505,#72506,#72507,#72508,#72509,#72510,#72511,#72512,#72513,#72514,#72515,
#72516,#72517,#72518,#72519,#72520,#72521,#72522,#72523,#72524,#72525,#72526,
#72527,#72528,#72529,#72530,#72531,#72532,#72533,#72534,#72535,#72536,#72537,
#72538,#72539,#72540,#72541,#72542,#72543,#72544,#72545,#72546,#72547,#72548,
#72549,#72550,#72551,#72552,#72553,#72554,#72555,#72556,#72557,#72558,#72559,
#72560,#72561,#72562,#72563,#72564,#72565,#72566,#72567,#72568,#72569,#72570,
#72571,#72572,#72573,#72574,#72575,#72576,#72577,#72578,#72579,#72580,#72581,
#72582,#72583,#72584,#72585,#72586,#72587,#72588,#72589,#72590,#72591,#72592,
#72593,#72594,#72595,#72596,#72597,#72598,#72599,#72600,#72601,#72602,#72603,
#72604,#72605,#72606,#72607,#72608,#72609,#72610,#72611,#72612,#72613,#72614,
#72615,#72616,#72617,#72618,#72619,#72620,#72621,#72622,#72623,#72624,#72625,
#72626,#72627,#72628,#72629,#72630,#72631,#72632,#72633,#72634,#72635,#72636,
#72637,#72638,#72639,#72640,#72641,#72642,#72643,#72644,#72645,#72646,#72647,
#72648,#72649,#72650,#72651,#72652,#72653,#72654,#72655,#72656,#72657,#72658,
#72659,#72660,#72661,#72662,#72663,#72664,#72665,#72666,#72667,#72668,#72669,
#72670,#72671,#72672,#72673,#72674,#72675,#72676,#72677,#72678,#72679,#72680,
#72681,#72682,#72683,#72684,#72685,#72686,#72687,#72688,#72689,#72690,#72691,
#72692,#72693,#72694,#72695,#72696,#72697,#72698,#72699,#72700,#72701,#72702,
#72703,#72704,#72705,#72706,#72707,#72708,#72709,#72710,#72711,#72712,#72713,
#72714,#72715,#72716,#72717,#72718,#72719,#72720,#72721,#72722,#72723,#72724,
#72725,#72726,#72727,#72728,#72729,#72730,#72731,#72732,#72733,#72734,#72735,
#72736,#72737,#72738,#72739,#72740,#72741,#72742,#72743,#72744,#72745,#72746,
#72747,#72748,#72749,#72750,#72751,#72752,#72753,#72754,#72755,#72756,#72757,
#72758,#72759,#72760,#72761,#72762,#72763,#72764,#72765,#72766,#72767,#72768,
#72769,#72770,#72771,#72772,#72773,#72774,#72775,#72776,#72777,#72778,#72779,
#72780,#72781,#72782,#72783,#72784,#72785,#72786,#72787,#72788,#72789,#72790,
#72791,#72792,#72793,#72794,#72795,#72796,#72797,#72798,#72799,#72800,#72801,
#72802,#72803,#72804,#72805,#72806,#72807,#72808,#72809,#72810,#72811,#72812,
#72813,#72814,#72815,#72816,#72817,#72818),(#72819,#72820,#72821,#72822,
#72823,#72824,#72825,#72826,#72827,#72828,#72829,#72830,#72831,#72832,#72833,
#72834,#72835,#72836,#72837,#72838,#72839,#72840,#72841,#72842,#72843,#72844,
#72845,#72846,#72847,#72848,#72849,#72850,#72851,#72852,#72853,#72854,#72855,
#72856,#72857,#72858,#72859,#72860,#72861,#72862,#72863,#72864,#72865,#72866,
#72867,#72868,#72869,#72870,#72871,#72872,#72873,#72874,#72875,#72876,#72877,
#72878,#72879,#72880,#72881,#72882,#72883,#72884,#72885,#72886,#72887,#72888,
#72889,#72890,#72891,#72892,#72893,#72894,#72895,#72896,#72897,#72898,#72899,
#72900,#72901,#72902,#72903,#72904,#72905,#72906,#72907,#72908,#72909,#72910,
#72911,#72912,#72913,#72914,#72915,#72916,#72917,#72918,#72919,#72920,#72921,
#72922,#72923,#72924,#72925,#72926,#72927,#72928,#72929,#72930,#72931,#72932,
#72933,#72934,#72935,#72936,#72937,#72938,#72939,#72940,#72941,#72942,#72943,
#72944,#72945,#72946,#72947,#72948,#72949,#72950,#72951,#72952,#72953,#72954,
#72955,#72956,#72957,#72958,#72959,#72960,#72961,#72962,#72963,#72964,#72965,
#72966,#72967,#72968,#72969,#72970,#72971,#72972,#72973,#72974,#72975,#72976,
#72977,#72978,#72979,#72980,#72981,#72982,#72983,#72984,#72985,#72986,#72987,
#72988,#72989,#72990,#72991,#72992,#72993,#72994,#72995,#72996,#72997,#72998,
#72999,#73000,#73001,#73002,#73003,#73004,#73005,#73006,#73007,#73008,#73009,
#73010,#73011,#73012,#73013,#73014,#73015,#73016,#73017,#73018,#73019,#73020,
#73021,#73022,#73023,#73024,#73025,#73026,#73027,#73028,#73029,#73030,#73031,
#73032,#73033,#73034,#73035,#73036,#73037,#73038,#73039,#73040,#73041,#73042,
#73043,#73044,#73045,#73046,#73047,#73048,#73049,#73050,#73051,#73052,#73053,
#73054,#73055,#73056,#73057,#73058,#73059,#73060,#73061,#73062,#73063,#73064,
#73065,#73066,#73067,#73068,#73069,#73070,#73071,#73072,#73073,#73074,#73075,
#73076,#73077,#73078,#73079,#73080,#73081,#73082,#73083,#73084,#73085,#73086,
#73087,#73088,#73089,#73090,#73091,#73092,#73093,#73094,#73095,#73096,#73097,
#73098,#73099,#73100,#73101,#73102,#73103,#73104,#73105,#73106,#73107,#73108,
#73109,#73110,#73111,#73112,#73113,#73114,#73115,#73116,#73117,#73118,#73119,
#73120,#73121,#73122,#73123,#73124,#73125,#73126,#73127,#73128,#73129,#73130,
#73131,#73132,#73133,#73134,#73135,#73136,#73137,#73138,#73139,#73140,#73141,
#73142,#73143,#73144,#73145,#73146,#73147,#73148,#73149,#73150,#73151,#73152,
#73153,#73154,#73155,#73156,#73157,#73158,#73159,#73160,#73161,#73162,#73163,
#73164,#73165,#73166,#73167,#73168,#73169,#73170,#73171,#73172,#73173,#73174,
#73175,#73176,#73177,#73178,#73179,#73180,#73181,#73182,#73183,#73184,#73185,
#73186,#73187,#73188,#73189,#73190,#73191,#73192,#73193,#73194,#73195,#73196,
#73197,#73198,#73199,#73200,#73201,#73202,#73203,#73204,#73205,#73206,#73207,
#73208,#73209,#73210,#73211,#73212,#73213,#73214,#73215,#73216,#73217,#73218,
#73219,#73220,#73221,#73222,#73223,#73224,#73225,#73226,#73227,#73228,#73229,
#73230,#73231,#73232,#73233,#73234,#73235,#73236,#73237,#73238,#73239,#73240,
#73241,#73242,#73243,#73244,#73245,#73246,#73247,#73248,#73249,#73250,#73251,
#73252,#73253,#73254,#73255,#73256,#73257,#73258,#73259,#73260,#73261,#73262,
#73263,#73264,#73265,#73266,#73267,#73268,#73269,#73270,#73271,#73272,#73273,
#73274,#73275,#73276,#73277,#73278,#73279,#73280,#73281,#73282,#73283,#73284,
#73285,#73286,#73287,#73288,#73289,#73290,#73291,#73292,#73293,#73294,#73295,
#73296,#73297,#73298,#73299,#73300,#73301,#73302,#73303,#73304,#73305,#73306,
#73307,#73308,#73309,#73310,#73311,#73312,#73313,#73314,#73315,#73316,#73317,
#73318,#73319,#73320,#73321,#73322,#73323,#73324,#73325,#73326,#73327,#73328,
#73329,#73330,#73331,#73332,#73333,#73334,#73335,#73336,#73337,#73338,#73339,
#73340,#73341,#73342,#73343,#73344,#73345,#73346,#73347,#73348,#73349,#73350,
#73351),(#73352,#73353,#73354,#73355,#73356,#73357,#73358,#73359,#73360,
#73361,#73362,#73363,#73364,#73365,#73366,#73367,#73368,#73369,#73370,#73371,
#73372,#73373,#73374,#73375,#73376,#73377,#73378,#73379,#73380,#73381,#73382,
#73383,#73384,#73385,#73386,#73387,#73388,#73389,#73390,#73391,#73392,#73393,
#73394,#73395,#73396,#73397,#73398,#73399,#73400,#73401,#73402,#73403,#73404,
#73405,#73406,#73407,#73408,#73409,#73410,#73411,#73412,#73413,#73414,#73415,
#73416,#73417,#73418,#73419,#73420,#73421,#73422,#73423,#73424,#73425,#73426,
#73427,#73428,#73429,#73430,#73431,#73432,#73433,#73434,#73435,#73436,#73437,
#73438,#73439,#73440,#73441,#73442,#73443,#73444,#73445,#73446,#73447,#73448,
#73449,#73450,#73451,#73452,#73453,#73454,#73455,#73456,#73457,#73458,#73459,
#73460,#73461,#73462,#73463,#73464,#73465,#73466,#73467,#73468,#73469,#73470,
#73471,#73472,#73473,#73474,#73475,#73476,#73477,#73478,#73479,#73480,#73481,
#73482,#73483,#73484,#73485,#73486,#73487,#73488,#73489,#73490,#73491,#73492,
#73493,#73494,#73495,#73496,#73497,#73498,#73499,#73500,#73501,#73502,#73503,
#73504,#73505,#73506,#73507,#73508,#73509,#73510,#73511,#73512,#73513,#73514,
#73515,#73516,#73517,#73518,#73519,#73520,#73521,#73522,#73523,#73524,#73525,
#73526,#73527,#73528,#73529,#73530,#73531,#73532,#73533,#73534,#73535,#73536,
#73537,#73538,#73539,#73540,#73541,#73542,#73543,#73544,#73545,#73546,#73547,
#73548,#73549,#73550,#73551,#73552,#73553,#73554,#73555,#73556,#73557,#73558,
#73559,#73560,#73561,#73562,#73563,#73564,#73565,#73566,#73567,#73568,#73569,
#73570,#73571,#73572,#73573,#73574,#73575,#73576,#73577,#73578,#73579,#73580,
#73581,#73582,#73583,#73584,#73585,#73586,#73587,#73588,#73589,#73590,#73591,
#73592,#73593,#73594,#73595,#73596,#73597,#73598,#73599,#73600,#73601,#73602,
#73603,#73604,#73605,#73606,#73607,#73608,#73609,#73610,#73611,#73612,#73613,
#73614,#73615,#73616,#73617,#73618,#73619,#73620,#73621,#73622,#73623,#73624,
#73625,#73626,#73627,#73628,#73629,#73630,#73631,#73632,#73633,#73634,#73635,
#73636,#73637,#73638,#73639,#73640,#73641,#73642,#73643,#73644,#73645,#73646,
#73647,#73648,#73649,#73650,#73651,#73652,#73653,#73654,#73655,#73656,#73657,
#73658,#73659,#73660,#73661,#73662,#73663,#73664,#73665,#73666,#73667,#73668,
#73669,#73670,#73671,#73672,#73673,#73674,#73675,#73676,#73677,#73678,#73679,
#73680,#73681,#73682,#73683,#73684,#73685,#73686,#73687,#73688,#73689,#73690,
#73691,#73692,#73693,#73694,#73695,#73696,#73697,#73698,#73699,#73700,#73701,
#73702,#73703,#73704,#73705,#73706,#73707,#73708,#73709,#73710,#73711,#73712,
#73713,#73714,#73715,#73716,#73717,#73718,#73719,#73720,#73721,#73722,#73723,
#73724,#73725,#73726,#73727,#73728,#73729,#73730,#73731,#73732,#73733,#73734,
#73735,#73736,#73737,#73738,#73739,#73740,#73741,#73742,#73743,#73744,#73745,
#73746,#73747,#73748,#73749,#73750,#73751,#73752,#73753,#73754,#73755,#73756,
#73757,#73758,#73759,#73760,#73761,#73762,#73763,#73764,#73765,#73766,#73767,
#73768,#73769,#73770,#73771,#73772,#73773,#73774,#73775,#73776,#73777,#73778,
#73779,#73780,#73781,#73782,#73783,#73784,#73785,#73786,#73787,#73788,#73789,
#73790,#73791,#73792,#73793,#73794,#73795,#73796,#73797,#73798,#73799,#73800,
#73801,#73802,#73803,#73804,#73805,#73806,#73807,#73808,#73809,#73810,#73811,
#73812,#73813,#73814,#73815,#73816,#73817,#73818,#73819,#73820,#73821,#73822,
#73823,#73824,#73825,#73826,#73827,#73828,#73829,#73830,#73831,#73832,#73833,
#73834,#73835,#73836,#73837,#73838,#73839,#73840,#73841,#73842,#73843,#73844,
#73845,#73846,#73847,#73848,#73849,#73850,#73851,#73852,#73853,#73854,#73855,
#73856,#73857,#73858,#73859,#73860,#73861,#73862,#73863,#73864,#73865,#73866,
#73867,#73868,#73869,#73870,#73871,#73872,#73873,#73874,#73875,#73876,#73877,
#73878,#73879,#73880,#73881,#73882,#73883,#73884)),.UNSPECIFIED.,.F.,.F.,
 .F.,(4,4),(4,1,1,1,1,1,1,1,1,1,1,1,1,1,1,1,1,1,1,1,1,1,1,1,1,1,1,1,1,1,
1,1,1,1,1,1,1,1,1,1,1,1,1,1,1,1,1,1,1,1,1,1,1,1,1,1,1,1,1,1,1,1,1,1,1,1,
1,1,1,1,1,1,1,1,1,1,1,1,1,1,1,1,1,1,1,1,1,1,1,1,1,1,1,1,1,1,1,1,1,1,1,1,
1,1,1,1,1,1,1,1,1,1,1,1,1,1,1,1,1,1,1,1,1,1,1,1,1,1,1,1,1,1,1,1,1,1,1,1,
1,1,1,1,1,1,1,1,1,1,1,1,1,1,1,1,1,1,1,1,1,1,1,1,1,1,1,1,1,1,1,1,1,1,1,1,
1,1,1,1,1,1,1,1,1,1,1,1,1,1,1,1,1,1,1,1,1,1,1,1,1,1,1,1,1,1,1,1,1,1,1,1,
1,1,1,1,1,1,1,1,1,1,1,1,1,1,1,1,1,1,1,1,1,1,1,1,1,1,1,1,1,1,1,1,1,1,1,1,
1,1,1,1,1,1,1,1,1,1,1,1,1,1,1,1,1,1,1,1,1,1,1,1,1,1,1,1,1,1,1,1,1,1,1,1,
1,1,1,1,1,1,1,1,1,1,1,1,1,1,1,1,1,1,1,1,1,1,1,1,1,1,1,1,1,1,1,1,1,1,1,1,
1,1,1,1,1,1,1,1,1,1,1,1,1,1,1,1,1,1,1,1,1,1,1,1,1,1,1,1,1,1,1,1,1,1,1,1,
1,1,1,1,1,1,1,1,1,1,1,1,1,1,1,1,1,1,1,1,1,1,1,1,1,1,1,1,1,1,1,1,1,1,1,1,
1,1,1,1,1,1,1,1,1,1,1,1,1,1,1,1,1,1,1,1,1,1,1,1,1,1,1,1,1,1,1,1,1,1,1,1,
1,1,1,1,1,1,1,1,1,1,1,1,1,1,1,1,1,1,1,1,1,1,1,1,1,1,1,1,1,1,1,1,1,1,1,1,
1,1,1,1,1,1,1,1,1,1,1,1,1,1,1,1,1,1,1,1,1,1,1,1,1,1,1,1,1,1,1,1,1,1,1,1,
1,1,1,1,1,1,1,1,1,1,1,1,1,1,1,1,1,1,1,1,1,1,1,1,1,1,1,1,1,1,1,1,4),(-0.000330931146184842,
0.0826790177557676),(11.6145478157386,12.6149288832288,13.6146435387017,
14.6143581941745,15.6140728496473,16.6137875051202,17.613502160593,18.6132168160658,
19.6129314715387,20.6126461270115,21.6123607824843,22.6120754379572,23.61179009343,
24.6115047489028,25.6112194043757,26.6109340598485,27.6106487153213,28.6103633707942,
29.610078026267,30.6097926817398,31.6095073372127,32.6092219926855,33.6089366481583,
34.6086513036311,35.608365959104,36.6080806145768,37.6077952700496,38.6075099255225,
39.6072245809953,40.6069392364681,41.606653891941,42.6063685474138,43.6060832028866,
44.6057978583595,45.6055125138323,46.6052271693051,47.604941824778,48.6046564802508,
49.6043711357236,50.6040857911965,51.6038004466693,52.6035151021421,53.603229757615,
54.6029444130878,55.6026590685606,56.6023737240335,57.6020883795063,58.6018030349791,
59.6015176904519,60.6012323459248,61.6009470013976,62.6006616568704,63.6003763123433,
64.6000909678161,65.5998056232889,66.5995202787618,67.5992349342346,68.5989495897074,
69.5986642451803,70.5983789006531,71.5980935561259,72.5978082115988,73.5975228670716,
74.5972375225444,75.5969521780173,76.5966668334901,77.5963814889629,78.5960961444358,
79.5958107999086,80.5955254553814,81.5952401108542,82.5949547663271,83.5946694217999,
84.5943840772727,85.5940987327456,86.5938133882184,87.5935280436913,88.5932426991641,
89.5929573546369,90.5926720101097,91.5923866655826,92.5921013210554,93.5918159765282,
94.5915306320011,95.5912452874739,96.5909599429467,97.5906745984196,98.5903892538924,
99.5901039093652,100.589818564838,101.589533220311,102.589247875784,103.588962531257,
104.588677186729,105.588391842202,106.588106497675,107.587821153148,108.587535808621,
109.587250464094,110.586965119566,111.586679775039,112.586394430512,113.586109085985,
114.585823741458,115.585538396931,116.585253052403,117.584967707876,118.584682363349,
119.584397018822,120.584111674295,121.583826329768,122.58354098524,123.583255640713,
124.582970296186,125.582684951659,126.582399607132,127.582114262605,128.581828918077,
129.58154357355,130.581258229023,131.580972884496,132.580687539969,133.580402195442,
134.580116850914,135.579831506387,136.57954616186,137.579260817333,138.578975472806,
139.578690128279,140.578404783751,141.578119439224,142.577834094697,143.57754875017,
144.577263405643,145.576978061116,146.576692716588,147.576407372061,148.576122027534,
149.575836683007,150.57555133848,151.575265993952,152.574980649425,153.574695304898,
154.574409960371,155.574124615844,156.573839271317,157.573553926789,158.573268582262,
159.572983237735,160.572697893208,161.572412548681,162.572127204154,163.571841859626,
164.571556515099,165.571271170572,166.570985826045,167.570700481518,168.570415136991,
169.570129792463,170.569844447936,171.569559103409,172.569273758882,173.568988414355,
174.568703069828,175.5684177253,176.568132380773,177.567847036246,178.567561691719,
179.567276347192,180.566991002665,181.566705658137,182.56642031361,183.566134969083,
184.565849624556,185.565564280029,186.565278935502,187.564993590974,188.564708246447,
189.56442290192,190.564137557393,191.563852212866,192.563566868339,193.563281523811,
194.562996179284,195.562710834757,196.56242549023,197.562140145703,198.561854801176,
199.561569456648,200.561284112121,201.560998767594,202.560713423067,203.56042807854,
204.560142734013,205.559857389485,206.559572044958,207.559286700431,208.559001355904,
209.558716011377,210.55843066685,211.558145322322,212.557859977795,213.557574633268,
214.557289288741,215.557003944214,216.556718599687,217.556433255159,218.556147910632,
219.555862566105,220.555577221578,221.555291877051,222.555006532524,223.554721187996,
224.554435843469,225.554150498942,226.553865154415,227.553579809888,228.553294465361,
229.553009120833,230.552723776306,231.552438431779,232.552153087252,233.551867742725,
234.551582398198,235.55129705367,236.551011709143,237.550726364616,238.550441020089,
239.550155675562,240.549870331035,241.549584986507,242.54929964198,243.549014297453,
244.548728952926,245.548443608399,246.548158263872,247.547872919344,248.547587574817,
249.54730223029,250.547016885763,251.546731541236,252.546446196709,253.546160852181,
254.545875507654,255.545590163127,256.5453048186,257.545019474073,258.544734129546,
259.544448785018,260.544163440491,261.543878095964,262.543592751437,263.54330740691,
264.543022062382,265.542736717855,266.542451373328,267.542166028801,268.541880684274,
269.541595339747,270.541309995219,271.541024650692,272.540739306165,273.540453961638,
274.540168617111,275.539883272584,276.539597928056,277.539312583529,278.539027239002,
279.538741894475,280.538456549948,281.538171205421,282.537885860893,283.537600516366,
284.537315171839,285.537029827312,286.536744482785,287.536459138258,288.53617379373,
289.535888449203,290.535603104676,291.535317760149,292.535032415622,293.534747071095,
294.534461726567,295.53417638204,296.533891037513,297.533605692986,298.533320348459,
299.533035003932,300.532749659404,301.532464314877,302.53217897035,303.531893625823,
304.531608281296,305.531322936769,306.531037592241,307.530752247714,308.530466903187,
309.53018155866,310.529896214133,311.529610869606,312.529325525078,313.529040180551,
314.528754836024,315.528469491497,316.52818414697,317.527898802443,318.527613457915,
319.527328113388,320.527042768861,321.526757424334,322.526472079807,323.52618673528,
324.525901390752,325.525616046225,326.525330701698,327.525045357171,328.524760012644,
329.524474668117,330.524189323589,331.523903979062,332.523618634535,333.523333290008,
334.523047945481,335.522762600954,336.522477256426,337.522191911899,338.521906567372,
339.521621222845,340.521335878318,341.521050533791,342.520765189263,343.520479844736,
344.520194500209,345.519909155682,346.519623811155,347.519338466628,348.5190531221,
349.518767777573,350.518482433046,351.518197088519,352.517911743992,353.517626399465,
354.517341054937,355.51705571041,356.516770365883,357.516485021356,358.516199676829,
359.515914332302,360.515628987774,361.515343643247,362.51505829872,363.514772954193,
364.514487609666,365.514202265139,366.513916920611,367.513631576084,368.513346231557,
369.51306088703,370.512775542503,371.512490197976,372.512204853448,373.511919508921,
374.511634164394,375.511348819867,376.51106347534,377.510778130813,378.510492786285,
379.510207441758,380.509922097231,381.509636752704,382.509351408177,383.509066063649,
384.508780719122,385.508495374595,386.508210030068,387.507924685541,388.507639341014,
389.507353996486,390.507068651959,391.506783307432,392.506497962905,393.506212618378,
394.505927273851,395.505641929323,396.505356584796,397.505071240269,398.504785895742,
399.504500551215,400.504215206688,401.50392986216,402.503644517633,403.503359173106,
404.503073828579,405.502788484052,406.502503139525,407.502217794997,408.50193245047,
409.501647105943,410.501361761416,411.501076416889,412.500791072362,413.500505727834,
414.500220383307,415.49993503878,416.499649694253,417.499364349726,418.499079005199,
419.498793660671,420.498508316144,421.498222971617,422.49793762709,423.497652282563,
424.497366938036,425.497081593508,426.496796248981,427.496510904454,428.496225559927,
429.4959402154,430.495654870873,431.495369526345,432.495084181818,433.494798837291,
434.494513492764,435.494228148237,436.49394280371,437.493657459182,438.493372114655,
439.493086770128,440.492801425601,441.492516081074,442.492230736547,443.491945392019,
444.491660047492,445.491374702965,446.491089358438,447.490804013911,448.490518669384,
449.490233324856,450.489947980329,451.489662635802,452.489377291275,453.489091946748,
454.488806602221,455.488521257693,456.488235913166,457.487950568639,458.487665224112,
459.487379879585,460.487094535058,461.48680919053,462.486523846003,463.486238501476,
464.485953156949,465.485667812422,466.485382467895,467.485097123367,468.48481177884,
469.484526434313,470.484241089786,471.483955745259,472.483670400732,473.483385056204,
474.483099711677,475.48281436715,476.482529022623,477.482243678096,478.481958333569,
479.481672989041,480.481387644514,481.481102299987,482.48081695546,483.480531610933,
484.480246266406,485.479960921878,486.479675577351,487.479390232824,488.479104888297,
489.47881954377,490.478534199243,491.478248854715,492.477963510188,493.477678165661,
494.477392821134,495.477107476607,496.47682213208,497.476536787552,498.476251443025,
499.475966098498,500.475680753971,501.475395409444,502.475110064917,503.474824720389,
504.474539375862,505.474254031335,506.473968686808,507.473683342281,508.473397997753,
509.473112653226,510.472827308699,511.472541964172,512.472256619645,513.471971275118,
514.471685930591,515.471400586063,516.471115241536,517.470829897009,518.470544552482,
519.470259207955,520.469973863428,521.4696885189,522.469403174373,523.469117829846,
524.468832485319,525.468547140792,526.468261796265,527.467976451737,528.46769110721,
529.467405762683,530.467120418156,531.466835073629,532.466549729102,533.466264384574,
534.465979040047,535.46569369552,536.465408350993,537.465123006466,538.464837661939,
539.464552317411,540.464266972884,541.463981628357),.UNSPECIFIED.);
#49=B_SPLINE_CURVE_WITH_KNOTS('',3,(#6229,#6230,#6231,#6232,#6233,#6234,
#6235,#6236,#6237,#6238,#6239,#6240,#6241,#6242,#6243,#6244,#6245,#6246,
#6247,#6248,#6249,#6250,#6251,#6252,#6253,#6254,#6255,#6256,#6257,#6258,
#6259,#6260,#6261,#6262,#6263,#6264,#6265,#6266,#6267,#6268,#6269,#6270,
#6271,#6272,#6273,#6274,#6275,#6276,#6277,#6278,#6279,#6280,#6281,#6282,
#6283,#6284,#6285,#6286,#6287,#6288,#6289,#6290,#6291,#6292,#6293,#6294,
#6295,#6296,#6297,#6298,#6299,#6300,#6301,#6302,#6303,#6304,#6305,#6306,
#6307,#6308,#6309,#6310,#6311,#6312,#6313,#6314,#6315,#6316,#6317,#6318,
#6319,#6320,#6321,#6322,#6323,#6324,#6325,#6326,#6327,#6328,#6329,#6330,
#6331,#6332,#6333,#6334,#6335,#6336,#6337,#6338,#6339,#6340),
 .UNSPECIFIED.,.F.,.F.,(4,3,3,3,3,3,3,3,3,3,3,3,3,3,3,3,3,3,3,3,3,3,3,3,
3,3,3,3,3,3,3,3,3,3,3,3,3,4),(10.3762600297592,10.4685665931634,10.5607519230172,
10.6548925221748,10.7469246166194,10.8389288274898,10.9309307648174,11.0266672526824,
11.1187945753552,11.21098417842,11.3033079207642,11.3138767162776,11.4071165017747,
11.5002333969254,11.5932547895379,11.6862120629539,11.7791363956122,11.8720524013631,
11.9649846805265,12.0580178810066,12.1511041087062,12.2443458788881,12.3135913717504,
12.4065309273335,12.4993426448501,12.5920543448581,12.6846963965842,12.7773022111874,
12.8698967723451,12.9625050478778,13.0552122586236,13.1479708846286,13.2408858091675,
13.3133060272232,13.4063880812434,13.4993598882143,13.5922296797452,13.6621187583616),
 .UNSPECIFIED.);
#50=B_SPLINE_CURVE_WITH_KNOTS('',3,(#6343,#6344,#6345,#6346,#6347,#6348,
#6349,#6350,#6351,#6352,#6353,#6354,#6355,#6356,#6357,#6358,#6359,#6360,
#6361,#6362,#6363,#6364,#6365,#6366,#6367,#6368,#6369,#6370,#6371,#6372,
#6373,#6374,#6375,#6376,#6377,#6378,#6379,#6380,#6381,#6382,#6383,#6384,
#6385,#6386,#6387,#6388,#6389,#6390,#6391,#6392,#6393,#6394,#6395,#6396,
#6397,#6398,#6399,#6400,#6401,#6402,#6403,#6404,#6405,#6406,#6407,#6408,
#6409,#6410,#6411,#6412),.UNSPECIFIED.,.F.,.F.,(4,3,3,3,3,3,3,3,3,3,3,3,
3,3,3,3,3,3,3,3,3,3,3,4),(11.615214227756,11.7104959116212,11.8057232883005,
11.9009184235368,11.9961303776916,12.0913569841311,12.1866182838285,12.2819343459706,
12.3773918355249,12.4729276001673,12.5686320048391,12.6149288832288,12.7070190024734,
12.7989699433795,12.8908105692998,12.9825692112577,13.074284158239,13.1659812591482,
13.2576863409985,13.3494866953367,13.4413348419307,13.5333428212227,13.6146435387017,
13.6618816120544),.UNSPECIFIED.);
#51=B_SPLINE_CURVE_WITH_KNOTS('',3,(#6418,#6419,#6420,#6421,#6422,#6423,
#6424,#6425,#6426,#6427,#6428,#6429,#6430,#6431,#6432,#6433,#6434,#6435,
#6436,#6437,#6438,#6439,#6440,#6441,#6442,#6443,#6444,#6445,#6446,#6447,
#6448,#6449,#6450,#6451,#6452,#6453,#6454,#6455,#6456,#6457,#6458,#6459,
#6460,#6461,#6462,#6463,#6464,#6465,#6466,#6467,#6468,#6469,#6470,#6471,
#6472,#6473,#6474,#6475,#6476,#6477,#6478,#6479,#6480,#6481,#6482,#6483,
#6484,#6485,#6486,#6487,#6488,#6489,#6490,#6491,#6492,#6493,#6494,#6495,
#6496,#6497,#6498,#6499,#6500,#6501,#6502,#6503,#6504,#6505,#6506,#6507,
#6508,#6509,#6510,#6511,#6512,#6513,#6514,#6515,#6516,#6517,#6518,#6519,
#6520,#6521,#6522,#6523,#6524,#6525,#6526,#6527,#6528,#6529,#6530,#6531,
#6532,#6533,#6534,#6535,#6536,#6537,#6538,#6539,#6540,#6541,#6542,#6543,
#6544,#6545,#6546,#6547,#6548,#6549,#6550,#6551,#6552,#6553,#6554,#6555,
#6556,#6557,#6558,#6559,#6560,#6561,#6562,#6563,#6564,#6565,#6566,#6567,
#6568,#6569,#6570,#6571,#6572,#6573,#6574,#6575,#6576,#6577,#6578,#6579,
#6580,#6581,#6582,#6583,#6584,#6585,#6586,#6587,#6588,#6589,#6590,#6591,
#6592,#6593,#6594,#6595,#6596,#6597,#6598,#6599,#6600,#6601,#6602,#6603,
#6604,#6605,#6606,#6607,#6608,#6609,#6610,#6611,#6612,#6613,#6614,#6615,
#6616,#6617,#6618,#6619,#6620,#6621,#6622,#6623,#6624,#6625,#6626,#6627,
#6628,#6629,#6630,#6631,#6632,#6633,#6634,#6635,#6636,#6637,#6638,#6639,
#6640,#6641),.UNSPECIFIED.,.F.,.F.,(4,2,2,2,2,2,2,2,2,2,2,2,2,2,2,2,2,2,
2,2,2,2,2,2,2,2,2,2,2,2,2,2,2,2,2,2,2,2,2,2,2,2,2,2,2,2,2,2,2,2,2,2,2,2,
2,2,2,2,2,2,2,2,2,2,2,2,2,2,2,2,2,2,2,2,2,2,2,2,2,2,2,2,2,2,2,2,2,2,2,2,
2,2,2,2,2,2,2,2,2,2,2,2,2,2,2,2,2,2,2,2,2,4),(-1.37050854120238,-1.33686904903339,
-1.33072403175994,-1.3288424066245,-1.32782554961424,-1.32684093532529,
-1.32565745787055,-1.32438895674942,-1.32241511154026,-1.31870205271146,
-1.28627791863757,-1.19926958768006,-1.16918622785395,-1.16721306646538,
-1.16646094713311,-1.16592393006015,-1.16541214936304,-1.16468441681,-1.16317092933403,
-1.14800714537606,-1.11834817571685,-1.0136951735994,-1.00754311183712,
-1.00566095854807,-1.00464417289918,-1.00373609491063,-1.00258295445742,
-1.00056264173604,-0.998101189694289,-0.993082440173186,-0.979991937626143,
-0.94892155709358,-0.854519963144241,-0.853262234263941,-0.851558616924278,
-0.850783309512972,-0.846170558774688,-0.844061146189821,-0.843287995728194,
-0.842745323028977,-0.842235931456424,-0.841523897978037,-0.840089157684197,
-0.82851852733971,-0.802213413640655,-0.791146689138107,-0.697761319418871,
-0.69575606688349,-0.691947664512984,-0.690830319699865,-0.684432465447507,
-0.682521001318348,-0.681384501819927,-0.680393748831362,-0.679164802063678,
-0.676799969115957,-0.673816631864688,-0.667310530459367,-0.648755647389044,
-0.612459523118121,-0.526346307995641,-0.526230332752949,-0.521572468867822,
-0.520511571556346,-0.519817869748106,-0.519312876766996,-0.518682589921299,
-0.517630001664061,-0.513738110463563,-0.486702008753863,-0.461910725925344,
-0.454196416613347,-0.447518154764842,-0.44163307395454,-0.421390758091795,
-0.378559862049454,-0.376244316775148,-0.372542987023873,-0.370309069712533,
-0.361945413504594,-0.360041423042474,-0.358795075578016,-0.357846978087917,
-0.356902683870432,-0.355246391938894,-0.350322464057847,-0.342892733340551,
-0.32080454515825,-0.277021714141936,-0.20291752202762,-0.198618262379819,
-0.197488127251727,-0.196834009920347,-0.196273762780795,-0.195586586322357,
-0.194270153380627,-0.186184436428434,-0.171723167580107,-0.0703203637749224,
-0.0647305693058463,-0.0591438239231535,-0.0571526928326631,-0.0527632841355329,
-0.039330003794461,-0.0370918086250107,-0.0357589772463339,-0.0347398117165327,
-0.0337993895037417,-0.0327331461366012,-0.0312440460767627,-0.0287420106566131,
-0.000966338742490973),.UNSPECIFIED.);
#52=B_SPLINE_CURVE_WITH_KNOTS('',3,(#6642,#6643,#6644,#6645,#6646,#6647,
#6648,#6649,#6650,#6651,#6652,#6653,#6654,#6655,#6656,#6657,#6658,#6659,
#6660,#6661,#6662,#6663,#6664,#6665,#6666,#6667,#6668,#6669,#6670,#6671,
#6672,#6673,#6674,#6675,#6676,#6677,#6678,#6679,#6680,#6681,#6682,#6683,
#6684,#6685,#6686,#6687,#6688,#6689,#6690,#6691,#6692,#6693,#6694,#6695,
#6696,#6697,#6698,#6699,#6700,#6701,#6702,#6703,#6704,#6705,#6706,#6707,
#6708),.UNSPECIFIED.,.F.,.F.,(4,3,3,3,3,3,3,3,3,3,3,3,3,3,3,3,3,3,3,3,3,
3,4),(13.6621187583616,13.7549005319316,13.8476657797449,13.9404392779984,
14.0335846291728,14.1264999104908,14.2197602965935,14.3130206826961,14.4061140507736,
14.49908173365,14.5919513377176,14.6847535760267,14.7775209326273,14.8702782077547,
14.963050186716,15.0559216401269,15.1488450689533,15.2419240039525,15.3127353381689,
15.4164785260033,15.5199069032915,15.6227703545641,15.7079632677646),
 .UNSPECIFIED.);
#53=B_SPLINE_CURVE_WITH_KNOTS('',3,(#6710,#6711,#6712,#6713,#6714,#6715,
#6716,#6717,#6718,#6719,#6720,#6721,#6722,#6723,#6724,#6725,#6726,#6727,
#6728,#6729,#6730,#6731,#6732,#6733,#6734,#6735,#6736,#6737,#6738,#6739,
#6740,#6741,#6742,#6743,#6744,#6745,#6746,#6747,#6748,#6749,#6750,#6751,
#6752,#6753,#6754,#6755,#6756,#6757,#6758,#6759,#6760,#6761,#6762,#6763,
#6764,#6765,#6766,#6767,#6768,#6769,#6770,#6771,#6772,#6773,#6774,#6775,
#6776,#6777,#6778,#6779),.UNSPECIFIED.,.F.,.F.,(4,3,3,3,3,3,3,3,3,3,3,3,
3,3,3,3,3,3,3,3,3,3,3,4),(13.6618816120544,13.755040813502,13.8480880614116,
13.943871828007,14.0367832476407,14.1296722777591,14.2225635417726,14.3154816579344,
14.4085037791136,14.5015885715,14.5948115027264,14.6143581941745,14.7075979796716,
14.8007148748224,14.8937362674349,14.9866935408508,15.0796178735092,15.1725338792599,
15.2654661584234,15.3584993589035,15.4515855866031,15.544827356785,15.6140728496473,
15.70796326795),.UNSPECIFIED.);
#54=B_SPLINE_CURVE_WITH_KNOTS('',3,(#6780,#6781,#6782,#6783,#6784,#6785,
#6786,#6787,#6788,#6789,#6790,#6791,#6792,#6793,#6794,#6795,#6796,#6797,
#6798,#6799,#6800,#6801,#6802,#6803,#6804,#6805,#6806,#6807,#6808,#6809,
#6810,#6811,#6812,#6813,#6814,#6815,#6816,#6817,#6818,#6819,#6820,#6821,
#6822,#6823,#6824,#6825,#6826,#6827,#6828,#6829,#6830,#6831,#6832,#6833,
#6834,#6835,#6836,#6837,#6838,#6839,#6840,#6841,#6842,#6843,#6844,#6845,
#6846,#6847,#6848,#6849,#6850,#6851,#6852,#6853,#6854,#6855,#6856,#6857,
#6858,#6859,#6860,#6861,#6862,#6863,#6864,#6865,#6866,#6867,#6868,#6869,
#6870,#6871,#6872,#6873,#6874,#6875,#6876,#6877,#6878,#6879,#6880,#6881,
#6882,#6883,#6884,#6885,#6886,#6887,#6888,#6889,#6890,#6891,#6892,#6893,
#6894,#6895,#6896,#6897,#6898,#6899,#6900,#6901,#6902,#6903,#6904,#6905,
#6906,#6907,#6908,#6909,#6910,#6911,#6912,#6913,#6914,#6915,#6916,#6917,
#6918,#6919,#6920,#6921,#6922,#6923,#6924,#6925,#6926,#6927,#6928,#6929,
#6930,#6931,#6932,#6933,#6934,#6935,#6936,#6937,#6938,#6939,#6940,#6941,
#6942,#6943,#6944,#6945,#6946,#6947,#6948,#6949,#6950,#6951,#6952,#6953,
#6954,#6955,#6956,#6957,#6958,#6959,#6960,#6961,#6962,#6963,#6964,#6965,
#6966,#6967,#6968,#6969,#6970,#6971,#6972,#6973,#6974,#6975,#6976,#6977,
#6978,#6979,#6980,#6981,#6982,#6983,#6984,#6985),.UNSPECIFIED.,.F.,.F.,
(4,2,2,2,2,2,2,2,2,2,2,2,2,2,2,2,2,2,2,2,2,2,2,2,2,2,2,2,2,2,2,2,2,2,2,
2,2,2,2,2,2,2,2,2,2,2,2,2,2,2,2,2,2,2,2,2,2,2,2,2,2,2,2,2,2,2,2,2,2,2,2,
2,2,2,2,2,2,2,2,2,2,2,2,2,2,2,2,2,2,2,2,2,2,2,2,2,2,2,2,2,2,2,4),(-4.06088750423127,
-3.98270680377003,-3.94902050874879,-3.93409679396766,-3.93173231106793,
-3.93050319997425,-3.92950573566426,-3.92851018028234,-3.92670761804885,
-3.92112233105714,-3.91621589067004,-3.91231513591603,-3.90979295400919,
-3.90855754571573,-3.90581624275564,-3.89863734561648,-3.80758676832066,
-3.79004338162275,-3.77660679586409,-3.77003879478894,-3.76880560729759,
-3.76825770336036,-3.76771751123279,-3.76717913951976,-3.7664216875051,
-3.76485491606738,-3.74853125028312,-3.74465622348553,-3.71561920182063,
-3.69457362358076,-3.64797354334687,-3.62313993854728,-3.6103993048201,
-3.60811419000323,-3.60689397465597,-3.60588689544302,-3.60486742733792,
-3.60298036921095,-3.59681251006346,-3.49391762777491,-3.46308145032798,
-3.45285932932485,-3.4493084620027,-3.447677660958,-3.44638470406621,-3.44570413703487,
-3.44514324778417,-3.44449194039282,-3.44337540036809,-3.43921909765203,
-3.37821818726799,-3.33515428180871,-3.29388134256588,-3.28737714752424,
-3.2855357866189,-3.28441486424675,-3.28340407126987,-3.28211496037622,
-3.27948937864557,-3.26356391662639,-3.26223176063392,-3.26027790675209,
-3.25718179573601,-3.25516490570098,-3.20437135341289,-3.1551247179711,
-3.13378540525712,-3.12788843578953,-3.12552012774694,-3.12431033772132,
-3.12329856556556,-3.12268249932224,-3.12211950360246,-3.12139626465456,
-3.1202377181613,-3.11424596499402,-3.11201577424126,-3.11011324882386,
-3.05696943428382,-3.00971316395337,-2.97065748142882,-2.96651050500656,
-2.96339939236119,-2.96201884361775,-2.96099595663445,-2.96004672655908,
-2.95875164760135,-2.9561977915361,-2.93537339284446,-2.93245578340497,
-2.8814031397907,-2.82524128965409,-2.80468746681851,-2.80249864285803,
-2.80135655517014,-2.80063314076899,-2.79996306429501,-2.79941399138725,
-2.79884711383219,-2.79779503118521,-2.79433434734377,-2.73746932256422,
-2.69251420336544),.UNSPECIFIED.);
#55=B_SPLINE_CURVE_WITH_KNOTS('',3,(#6990,#6991,#6992,#6993,#6994,#6995,
#6996,#6997,#6998,#6999,#7000,#7001,#7002,#7003,#7004,#7005,#7006,#7007,
#7008,#7009,#7010,#7011,#7012,#7013,#7014,#7015,#7016,#7017,#7018,#7019,
#7020,#7021,#7022,#7023,#7024,#7025,#7026,#7027,#7028,#7029,#7030,#7031,
#7032,#7033,#7034,#7035,#7036,#7037,#7038,#7039,#7040,#7041,#7042,#7043,
#7044,#7045,#7046,#7047,#7048,#7049,#7050,#7051,#7052,#7053,#7054,#7055,
#7056,#7057,#7058,#7059,#7060,#7061,#7062,#7063,#7064,#7065,#7066,#7067,
#7068,#7069,#7070,#7071,#7072,#7073,#7074,#7075,#7076,#7077,#7078,#7079,
#7080,#7081,#7082,#7083,#7084,#7085,#7086,#7087,#7088,#7089,#7090,#7091,
#7092,#7093,#7094,#7095,#7096,#7097,#7098,#7099,#7100,#7101,#7102,#7103,
#7104,#7105,#7106,#7107,#7108,#7109,#7110,#7111,#7112,#7113,#7114,#7115,
#7116,#7117,#7118,#7119,#7120,#7121,#7122,#7123,#7124,#7125,#7126,#7127,
#7128,#7129,#7130,#7131,#7132,#7133,#7134,#7135,#7136,#7137,#7138,#7139,
#7140,#7141,#7142,#7143,#7144,#7145,#7146,#7147,#7148,#7149,#7150,#7151,
#7152,#7153,#7154,#7155,#7156,#7157,#7158,#7159,#7160,#7161,#7162,#7163,
#7164,#7165,#7166,#7167,#7168,#7169,#7170,#7171,#7172,#7173,#7174,#7175,
#7176,#7177,#7178,#7179,#7180,#7181,#7182,#7183,#7184,#7185,#7186,#7187,
#7188,#7189,#7190,#7191,#7192,#7193,#7194,#7195,#7196,#7197,#7198,#7199,
#7200,#7201,#7202,#7203,#7204,#7205,#7206,#7207,#7208,#7209,#7210,#7211,
#7212,#7213,#7214,#7215,#7216,#7217,#7218,#7219,#7220,#7221,#7222,#7223,
#7224,#7225,#7226,#7227,#7228,#7229,#7230,#7231,#7232,#7233,#7234,#7235,
#7236,#7237,#7238,#7239,#7240,#7241,#7242,#7243,#7244,#7245,#7246,#7247,
#7248,#7249,#7250,#7251,#7252,#7253,#7254,#7255,#7256,#7257,#7258,#7259,
#7260,#7261,#7262,#7263,#7264,#7265,#7266,#7267,#7268,#7269,#7270,#7271,
#7272,#7273,#7274,#7275,#7276,#7277,#7278,#7279,#7280,#7281,#7282,#7283,
#7284,#7285,#7286,#7287,#7288,#7289,#7290,#7291,#7292,#7293,#7294,#7295),
 .UNSPECIFIED.,.F.,.F.,(4,2,2,2,2,2,2,2,2,2,2,2,2,2,2,2,2,2,2,2,2,2,2,2,
2,2,2,2,2,2,2,2,2,2,2,2,2,2,2,2,2,2,2,2,2,2,2,2,2,2,2,2,2,2,2,2,2,2,2,2,
2,2,2,2,2,2,2,2,2,2,2,2,2,2,2,2,2,2,2,2,2,2,2,2,2,2,2,2,2,2,2,2,2,2,2,2,
2,2,2,2,2,2,2,2,2,2,2,2,2,2,2,2,2,2,2,2,2,2,2,2,2,2,2,2,2,2,2,2,2,2,2,2,
2,2,2,2,2,2,2,2,2,2,2,2,2,2,2,2,2,2,2,2,4),(-3.4011377333033,-3.36823275924315,
-3.32533821537189,-3.27265437450256,-3.26865604607521,-3.26712639407524,
-3.2660739058206,-3.265043853067,-3.26380381678253,-3.26071400730694,-3.23220829558781,
-3.15095176434001,-3.12670411423292,-3.11475843323702,-3.1095136941263,
-3.10734121394413,-3.10620484611436,-3.10548345364643,-3.10481468339031,
-3.10429026756391,-3.10372889855353,-3.10270445685079,-3.09947053752061,
-3.04465964380899,-2.99454811141961,-2.96197290683038,-2.94728522867798,
-2.94491569875493,-2.94367932266106,-2.94267361224274,-2.94166786225046,
-2.93984131905043,-2.93414075334494,-2.93199195630718,-2.93160372108128,
-2.92851576866371,-2.92529794307563,-2.92322211794468,-2.9214532133722,
-2.91788094095474,-2.91376041243119,-2.83684897212456,-2.78518882672316,
-2.78368387208337,-2.7828098117944,-2.78203145617703,-2.78146702604608,
-2.78094044604795,-2.78022822524511,-2.77884177618253,-2.76833995864156,
-2.76641873406103,-2.76596119188914,-2.76472792758538,-2.76410563134707,
-2.69643998339443,-2.66153335048973,-2.63677116201241,-2.62412549906813,
-2.62184887722492,-2.62063216696009,-2.619724946571,-2.61858923324097,-2.61668153574633,
-2.61031680908487,-2.60636053074062,-2.60453904677733,-2.60198303071082,
-2.60152037623093,-2.59792402391556,-2.59672914490128,-2.59521926603126,
-2.58879152634298,-2.49809378839896,-2.47777153010542,-2.46279548833425,
-2.46097426568099,-2.45997357685033,-2.45930908792335,-2.45868089262802,
-2.45813218770527,-2.45743330613678,-2.45635570409385,-2.45148937546274,
-2.36098632184745,-2.33635010651568,-2.3128519701406,-2.30092112236153,
-2.29868134046041,-2.29747248323213,-2.29647745532457,-2.29545743433319,
-2.29356051817955,-2.28728834135306,-2.18099183893918,-2.16118010117057,
-2.14190503157979,-2.13721228745901,-2.1360907578785,-2.13544529991579,
-2.13488394985283,-2.13418459046293,-2.1331055409029,-2.12822180998189,
-2.032103268204,-1.9795721898221,-1.97611649381286,-1.97478101856965,-1.97382020337401,
-1.97280157186733,-1.97145534867438,-1.9685365723614,-1.92259296791803,
-1.87159625811684,-1.83509096392933,-1.83051685145161,-1.82919163820721,
-1.82886588656804,-1.82786851269959,-1.82748621335548,-1.82671557103509,
-1.81485654514485,-1.81342044189802,-1.8126954739005,-1.81216559767254,
-1.81159218325346,-1.81080431591203,-1.80896805578428,-1.80646730613653,
-1.71769871049646,-1.65712461093832,-1.65320117553788,-1.65179181790613,
-1.65081095645836,-1.6498204432176,-1.648568924652,-1.64720618779517,-1.64500858022436,
-1.64070728726306,-1.59914549485817,-1.54797600162877,-1.50528006205352,
-1.50276683936719,-1.49171924381045,-1.49017615949073,-1.48943945626034,
-1.48887237287596,-1.48825567194553,-1.48726262420503,-1.48394832870727,
-1.46329367104304,-1.44475410509111,-1.37050854120238),.UNSPECIFIED.);
#56=B_SPLINE_CURVE_WITH_KNOTS('',3,(#7296,#7297,#7298,#7299,#7300,#7301,
#7302,#7303,#7304,#7305,#7306,#7307,#7308,#7309,#7310,#7311,#7312,#7313,
#7314,#7315,#7316,#7317,#7318,#7319,#7320,#7321,#7322,#7323,#7324,#7325,
#7326,#7327,#7328,#7329,#7330,#7331,#7332,#7333,#7334,#7335,#7336,#7337,
#7338,#7339,#7340,#7341,#7342,#7343,#7344,#7345,#7346,#7347,#7348,#7349,
#7350,#7351,#7352,#7353,#7354,#7355,#7356,#7357,#7358,#7359,#7360,#7361,
#7362,#7363,#7364,#7365,#7366,#7367,#7368,#7369,#7370,#7371,#7372,#7373,
#7374,#7375,#7376,#7377,#7378,#7379,#7380,#7381,#7382,#7383,#7384,#7385,
#7386,#7387,#7388,#7389,#7390,#7391,#7392,#7393,#7394,#7395,#7396,#7397,
#7398,#7399,#7400,#7401,#7402,#7403,#7404,#7405,#7406,#7407,#7408,#7409,
#7410,#7411,#7412,#7413,#7414,#7415,#7416,#7417,#7418,#7419,#7420,#7421,
#7422,#7423,#7424,#7425,#7426,#7427,#7428,#7429,#7430,#7431,#7432,#7433,
#7434,#7435,#7436,#7437,#7438,#7439,#7440,#7441,#7442,#7443,#7444,#7445,
#7446,#7447,#7448,#7449,#7450,#7451,#7452,#7453,#7454,#7455,#7456,#7457,
#7458,#7459,#7460,#7461,#7462,#7463,#7464,#7465,#7466,#7467,#7468,#7469,
#7470,#7471,#7472,#7473,#7474,#7475,#7476,#7477,#7478,#7479,#7480,#7481,
#7482,#7483,#7484,#7485,#7486,#7487,#7488,#7489,#7490,#7491,#7492,#7493,
#7494,#7495,#7496,#7497,#7498,#7499,#7500,#7501,#7502,#7503,#7504,#7505,
#7506,#7507,#7508,#7509,#7510,#7511,#7512,#7513,#7514,#7515,#7516,#7517,
#7518,#7519,#7520,#7521,#7522,#7523,#7524,#7525,#7526,#7527,#7528,#7529,
#7530,#7531,#7532,#7533,#7534,#7535,#7536,#7537,#7538,#7539,#7540,#7541,
#7542,#7543,#7544,#7545,#7546,#7547,#7548,#7549,#7550,#7551,#7552,#7553,
#7554,#7555,#7556,#7557,#7558,#7559,#7560,#7561,#7562,#7563),
 .UNSPECIFIED.,.F.,.F.,(4,2,2,2,2,2,2,2,2,2,2,2,2,2,2,2,2,2,2,2,2,2,2,2,
2,2,2,2,2,2,2,2,2,2,2,2,2,2,2,2,2,2,2,2,2,2,2,2,2,2,2,2,2,2,2,2,2,2,2,2,
2,2,2,2,2,2,2,2,2,2,2,2,2,2,2,2,2,2,2,2,2,2,2,2,2,2,2,2,2,2,2,2,2,2,2,2,
2,2,2,2,2,2,2,2,2,2,2,2,2,2,2,2,2,2,2,2,2,2,2,2,2,2,2,2,2,2,2,2,2,2,2,2,
2,4),(-2.69251420336544,-2.68743982535714,-2.65670177515205,-2.64243281012259,
-2.64008073513957,-2.63884792231432,-2.63784229275467,-2.63683426427094,
-2.63499691828289,-2.62921290210747,-2.51143796312435,-2.48004853099937,
-2.47865904349976,-2.47783210181189,-2.47708786259477,-2.47652916151592,
-2.47599386585528,-2.47524827367568,-2.47331619898672,-2.44599466435854,
-2.35668072882398,-2.33189655382166,-2.31921224504848,-2.31693399151984,
-2.31571706237886,-2.3148099609339,-2.31381865280317,-2.3120635098971,-2.30689736605355,
-2.22623717162586,-2.18360411974992,-2.16439293879996,-2.15594739736146,
-2.1546152455268,-2.15392442368147,-2.15336391139615,-2.15271262869491,
-2.15159371303526,-2.14740359044218,-2.07653151215772,-2.0314321842155,
-2.01934157870124,-2.01594347965038,-2.01286236046132,-1.99679998770164,
-1.99416828925841,-1.99287827098515,-1.99186772900896,-1.99074807308968,
-1.98891104724204,-1.98244468198175,-1.94156700420968,-1.89078621850982,
-1.83588688648386,-1.83251607524864,-1.83147484998298,-1.83091017756209,
-1.83040554070078,-1.82973706651059,-1.8285100164995,-1.82224745656665,
-1.80971373122685,-1.78612899253336,-1.67856948429592,-1.67242843821675,
-1.67054751116332,-1.66953091806029,-1.66852640434665,-1.66733340638653,
-1.6651348378526,-1.66240542810702,-1.60674448273095,-1.52135221251814,
-1.51027509585722,-1.50873099538414,-1.50799415273625,-1.50742714350185,
-1.50681077345624,-1.50581859792568,-1.50251024972305,-1.48191202369889,
-1.46051674485748,-1.35552683343781,-1.34934410262455,-1.34745832000521,
-1.34644082583539,-1.34544611770702,-1.34425915877244,-1.3420869824649,
-1.33939755051221,-1.28717929727067,-1.191452680538,-1.18653362244472,-1.18545204534978,
-1.18475205439321,-1.18419087652432,-1.18354637425512,-1.18242834828442,
-1.1777755789512,-1.15443954878669,-1.10891751165469,-1.07967579614171,
-1.02894701027745,-1.02551165061383,-1.02417976765711,-1.02322008538327,
-1.02220131377168,-1.02087964575332,-1.01806464060844,-1.01436656814974,
-1.00568249936415,-0.985107469143868,-0.935354203012806,-0.875932703915884,
-0.864292370535118,-0.862864123902574,-0.862141248974212,-0.861612002916771,
-0.861038348984915,-0.860248572322031,-0.85840077336365,-0.810428042730951,
-0.740767073980838,-0.705665428428054,-0.70247901695341,-0.701189372013492,
-0.700240680139341,-0.699280419850705,-0.697957571269769,-0.695136013903449,
-0.691427643732457,-0.682711188630784,-0.664998255990807,-0.662324499038495),
 .UNSPECIFIED.);
#57=B_SPLINE_CURVE_WITH_KNOTS('',3,(#7569,#7570,#7571,#7572,#7573,#7574,
#7575,#7576,#7577,#7578,#7579,#7580,#7581,#7582,#7583,#7584,#7585,#7586,
#7587,#7588,#7589,#7590,#7591,#7592,#7593,#7594,#7595,#7596,#7597,#7598,
#7599,#7600,#7601,#7602,#7603,#7604,#7605,#7606,#7607,#7608,#7609,#7610,
#7611,#7612,#7613,#7614,#7615,#7616,#7617,#7618,#7619,#7620,#7621,#7622,
#7623,#7624,#7625,#7626,#7627,#7628,#7629,#7630,#7631,#7632,#7633,#7634,
#7635,#7636,#7637,#7638,#7639,#7640,#7641,#7642,#7643,#7644,#7645,#7646,
#7647,#7648,#7649,#7650,#7651,#7652,#7653,#7654,#7655,#7656,#7657,#7658,
#7659,#7660,#7661,#7662,#7663,#7664,#7665,#7666,#7667,#7668,#7669,#7670,
#7671,#7672,#7673,#7674,#7675,#7676,#7677,#7678,#7679,#7680,#7681,#7682,
#7683,#7684,#7685,#7686,#7687,#7688,#7689,#7690,#7691,#7692,#7693,#7694,
#7695,#7696,#7697,#7698,#7699,#7700,#7701,#7702,#7703,#7704,#7705,#7706,
#7707,#7708,#7709,#7710,#7711,#7712,#7713,#7714,#7715,#7716,#7717,#7718,
#7719,#7720,#7721,#7722,#7723,#7724,#7725,#7726,#7727,#7728,#7729,#7730,
#7731,#7732,#7733,#7734,#7735,#7736,#7737,#7738,#7739,#7740,#7741,#7742,
#7743,#7744,#7745,#7746,#7747,#7748,#7749,#7750,#7751,#7752,#7753,#7754,
#7755,#7756,#7757,#7758,#7759,#7760,#7761,#7762,#7763,#7764,#7765,#7766,
#7767,#7768,#7769,#7770,#7771,#7772,#7773,#7774,#7775,#7776,#7777,#7778,
#7779,#7780,#7781,#7782),.UNSPECIFIED.,.F.,.F.,(4,2,2,2,2,2,2,2,2,2,2,2,
2,2,2,2,2,2,2,2,2,2,2,2,2,2,2,2,2,2,2,2,2,2,2,2,2,2,2,2,2,2,2,2,2,2,2,2,
2,2,2,2,2,2,2,2,2,2,2,2,2,2,2,2,2,2,2,2,2,2,2,2,2,2,2,2,2,2,2,2,2,2,2,2,
2,2,2,2,2,2,2,2,2,2,2,2,2,2,2,2,2,2,2,2,2,2,4),(-1.3701619549454,-1.34115135310392,
-1.31831143699482,-1.30718929834551,-1.30564344268663,-1.30490626846844,
-1.30435218608931,-1.30375216196324,-1.3031277417398,-1.30222323139391,
-1.30064309239597,-1.24528350026959,-1.15177538253259,-1.14613845984611,
-1.1443203021435,-1.14331636224977,-1.14231064046418,-1.14107155873233,
-1.13868849943003,-1.12366248269812,-1.08974344022715,-0.987868290400893,
-0.986822996530763,-0.983186710591633,-0.982113951081348,-0.981542821111783,
-0.98099365147284,-0.980329445335926,-0.979614060402389,-0.978492035852106,
-0.976357342255281,-0.971236116919608,-0.955627814543821,-0.934846726973935,
-0.852954257674139,-0.825111183074129,-0.822039555561863,-0.820802474280758,
-0.819773155029944,-0.818719659790828,-0.81718534091166,-0.813156739775617,
-0.758839966014531,-0.747758346212163,-0.665010199820993,-0.660321635888516,
-0.659258604637777,-0.65856430707468,-0.658015962476613,-0.657384888306055,
-0.656716066726844,-0.65570497956919,-0.653857248037782,-0.649645546401276,
-0.636737810240214,-0.612905633827277,-0.506307326496183,-0.499990038807665,
-0.498088066322018,-0.496953741209485,-0.496046491865546,-0.494828274735134,
-0.492544085647648,-0.479740753278492,-0.454951691761461,-0.426336711451099,
-0.417587091025077,-0.410178173361807,-0.403755795062053,-0.382479796443228,
-0.350300316886761,-0.337965584207506,-0.336513557558312,-0.335784655597205,
-0.335253856673224,-0.334692898554503,-0.333933312413152,-0.333085051521418,
-0.331643159827392,-0.32863425489269,-0.320470219075656,-0.29463715519072,
-0.204446540705489,-0.198191257648153,-0.196622558825525,-0.195413048405089,
-0.194131911134594,-0.178294807567187,-0.175674360440021,-0.174386559422068,
-0.173376236049085,-0.172255261325581,-0.170412504796756,-0.163890267301671,
-0.12241414700715,-0.0246162518267315,-0.0211795458601249,-0.0194053746103256,
-0.0142397686502214,-0.0131389262299117,-0.0124329152529533,-0.011900026942397,
-0.0113735739312462,-0.0107535690494248,-0.00985983528173989,-0.00681011635358851,
-0.000961031473661812),.UNSPECIFIED.);
#58=B_SPLINE_CURVE_WITH_KNOTS('',3,(#7783,#7784,#7785,#7786,#7787,#7788,
#7789,#7790,#7791,#7792,#7793,#7794,#7795,#7796,#7797,#7798,#7799,#7800,
#7801,#7802,#7803,#7804,#7805,#7806,#7807,#7808,#7809,#7810,#7811,#7812,
#7813,#7814,#7815,#7816,#7817,#7818,#7819,#7820,#7821,#7822,#7823,#7824,
#7825,#7826,#7827,#7828,#7829,#7830,#7831,#7832,#7833,#7834,#7835,#7836,
#7837,#7838,#7839,#7840,#7841,#7842,#7843,#7844,#7845,#7846,#7847,#7848,
#7849,#7850,#7851,#7852,#7853,#7854,#7855,#7856,#7857,#7858,#7859,#7860,
#7861,#7862,#7863,#7864,#7865,#7866,#7867,#7868,#7869,#7870,#7871,#7872,
#7873,#7874,#7875,#7876,#7877,#7878),.UNSPECIFIED.,.F.,.F.,(4,2,2,2,2,2,
2,2,2,2,2,2,2,2,2,2,2,2,2,2,2,2,2,2,2,2,2,2,2,2,2,2,2,2,2,2,2,2,2,2,2,2,
2,2,2,2,2,4),(-4.06232412567137,-3.96648542039376,-3.91745202059908,-3.91421284775563,
-3.9128083751604,-3.91178041528948,-3.91083535965951,-3.90955947355159,
-3.9064506929146,-3.8747357219951,-3.78887590179063,-3.7756751336445,-3.76010141945642,
-3.75519218831468,-3.75312329102701,-3.75202650859378,-3.75109128955129,
-3.7504930279537,-3.74993642574647,-3.74919383136785,-3.74756103250365,
-3.73466055024734,-3.70723196379845,-3.68300067981111,-3.63224595767332,
-3.59793957823797,-3.5921300575717,-3.59036326721542,-3.58925927663615,
-3.58824463406113,-3.58694545772515,-3.58419647026443,-3.56559655365699,
-3.56409065731819,-3.55754880898839,-3.46820308152277,-3.44286360191163,
-3.43422314357478,-3.43108660190526,-3.42959997565459,-3.42873342317246,
-3.42796037449361,-3.42739701062215,-3.42686930655741,-3.42615245717212,
-3.42474780319502,-3.41376750612561,-3.4011377333033),.UNSPECIFIED.);
#59=B_SPLINE_CURVE_WITH_KNOTS('',3,(#7880,#7881,#7882,#7883,#7884,#7885,
#7886,#7887,#7888,#7889,#7890,#7891,#7892,#7893,#7894,#7895,#7896,#7897,
#7898,#7899,#7900,#7901,#7902,#7903,#7904,#7905,#7906,#7907,#7908,#7909,
#7910,#7911,#7912,#7913,#7914,#7915,#7916,#7917,#7918,#7919,#7920,#7921,
#7922,#7923,#7924,#7925,#7926,#7927,#7928,#7929,#7930,#7931,#7932,#7933,
#7934,#7935,#7936,#7937,#7938,#7939,#7940,#7941,#7942,#7943,#7944,#7945,
#7946,#7947,#7948,#7949,#7950,#7951,#7952,#7953,#7954,#7955,#7956,#7957,
#7958,#7959,#7960,#7961,#7962,#7963,#7964,#7965,#7966,#7967,#7968,#7969,
#7970,#7971,#7972,#7973,#7974,#7975,#7976,#7977),.UNSPECIFIED.,.F.,.F.,
(4,2,2,2,2,2,2,2,2,2,2,2,2,2,2,2,2,2,2,2,2,2,2,2,2,2,2,2,2,2,2,2,2,2,2,
2,2,2,2,2,2,2,2,2,2,2,2,2,4),(-0.662324499038495,-0.626175222042389,-0.552344439691317,
-0.54131308533216,-0.539906618530502,-0.539189281204045,-0.538661429449004,
-0.538086599985878,-0.537290470234446,-0.535406146089974,-0.500679915735166,
-0.491155572976965,-0.483490151623553,-0.477046575968648,-0.471502134149543,
-0.425114532282901,-0.411311074824101,-0.382554733539475,-0.379498385594101,
-0.378243028774384,-0.377302877209851,-0.376347958398889,-0.375341429865526,
-0.372969289010916,-0.358026215372137,-0.32436524713951,-0.308620889977391,
-0.222511483520392,-0.22214655906175,-0.22131142190472,-0.217568310114071,
-0.216483410522155,-0.215909810754102,-0.215405633767391,-0.214749497017367,
-0.213579298370337,-0.208222875361436,-0.126052566752693,-0.108774115850613,
-0.102898337167071,-0.0599323184146636,-0.0566002057968977,-0.0552854519641184,
-0.0543301611443897,-0.0533086148152846,-0.0523063404258367,-0.0509863049470586,
-0.0488902604045168,-0.000961571770198283),.UNSPECIFIED.);
#60=B_SPLINE_CURVE_WITH_KNOTS('',3,(#7978,#7979,#7980,#7981,#7982,#7983,
#7984,#7985,#7986,#7987,#7988,#7989,#7990,#7991,#7992,#7993,#7994,#7995,
#7996,#7997,#7998,#7999,#8000,#8001,#8002,#8003,#8004,#8005,#8006,#8007,
#8008,#8009,#8010,#8011,#8012,#8013,#8014,#8015,#8016,#8017,#8018,#8019,
#8020,#8021,#8022,#8023,#8024,#8025,#8026,#8027,#8028,#8029,#8030,#8031,
#8032,#8033,#8034,#8035,#8036,#8037,#8038,#8039,#8040,#8041,#8042,#8043,
#8044,#8045,#8046,#8047,#8048,#8049,#8050,#8051,#8052,#8053,#8054,#8055,
#8056,#8057,#8058,#8059,#8060,#8061,#8062,#8063,#8064,#8065,#8066,#8067,
#8068,#8069,#8070,#8071,#8072,#8073,#8074,#8075,#8076,#8077,#8078,#8079,
#8080,#8081,#8082,#8083,#8084,#8085,#8086,#8087,#8088,#8089,#8090,#8091,
#8092,#8093,#8094,#8095,#8096,#8097,#8098,#8099,#8100,#8101,#8102,#8103,
#8104,#8105,#8106,#8107,#8108,#8109,#8110,#8111,#8112,#8113,#8114,#8115,
#8116,#8117,#8118,#8119,#8120,#8121,#8122,#8123,#8124,#8125,#8126,#8127,
#8128,#8129,#8130,#8131,#8132,#8133,#8134,#8135,#8136,#8137,#8138,#8139,
#8140,#8141,#8142,#8143,#8144,#8145,#8146,#8147,#8148,#8149,#8150,#8151,
#8152,#8153,#8154,#8155),.UNSPECIFIED.,.F.,.F.,(4,2,2,2,2,2,2,2,2,2,2,2,
2,2,2,2,2,2,2,2,2,2,2,2,2,2,2,2,2,2,2,2,2,2,2,2,2,2,2,2,2,2,2,2,2,2,2,2,
2,2,2,2,2,2,2,2,2,2,2,2,2,2,2,2,2,2,2,2,2,2,2,2,2,2,2,2,2,2,2,2,2,2,2,2,
2,2,2,2,4),(-4.06054529852164,-3.98499342916419,-3.96351933523899,-3.95458984271673,
-3.95323878401419,-3.95254398434728,-3.95203688610906,-3.95148678706787,
-3.95051806646734,-3.94770210468645,-3.90001299330774,-3.84766270383631,
-3.82771146819536,-3.79595055807878,-3.79302160190387,-3.79195328463526,
-3.7910119860081,-3.78999227252994,-3.78866075176049,-3.78584856748139,
-3.76480733076895,-3.76223716102674,-3.74640747779537,-3.7210404799264,
-3.70226630622101,-3.66438359736754,-3.64155118912963,-3.63182187502163,
-3.63044238804677,-3.62974169932912,-3.62923388473046,-3.62868651327399,
-3.6277313640613,-3.62501262598604,-3.62256216102106,-3.53672861148087,
-3.50251456318248,-3.48236223092972,-3.47180603464155,-3.46965169258818,
-3.46866804518156,-3.46769606043423,-3.4667298715607,-3.4653734753377,-3.46257824363259,
-3.43347623187295,-3.38507497476963,-3.34963539046534,-3.32727707081713,
-3.31681389342674,-3.30882084993112,-3.30750761579816,-3.30682078487585,
-3.30626048572905,-3.30560598286827,-3.30447325828035,-3.30014349969786,
-3.22589303350608,-3.17725600621282,-3.15877126067808,-3.15228340077766,
-3.1493063812167,-3.14694759491979,-3.1457191457725,-3.14480787156796,-3.14383417408783,
-3.14245006371774,-3.13868966235461,-3.05957683303757,-3.01421957331284,
-2.99019544265606,-2.98554901355322,-2.98443154252778,-2.98378719074342,
-2.98322603903951,-2.98252594638656,-2.98144396557571,-2.97651924030072,
-2.88158371114211,-2.8286678032174,-2.82597007868055,-2.82379545857293,
-2.8226063431288,-2.82169971238678,-2.82056255518472,-2.8186472056681,-2.81221278259547,
-2.70676879774558,-2.6920647855843),.UNSPECIFIED.);
#61=B_SPLINE_CURVE_WITH_KNOTS('',3,(#8160,#8161,#8162,#8163,#8164,#8165,
#8166,#8167,#8168,#8169,#8170,#8171,#8172,#8173,#8174,#8175,#8176,#8177,
#8178,#8179,#8180,#8181,#8182,#8183,#8184,#8185,#8186,#8187,#8188,#8189,
#8190,#8191,#8192,#8193,#8194,#8195,#8196,#8197,#8198,#8199,#8200,#8201,
#8202,#8203,#8204,#8205,#8206,#8207,#8208,#8209,#8210,#8211,#8212,#8213,
#8214,#8215,#8216,#8217,#8218,#8219,#8220,#8221,#8222,#8223,#8224,#8225,
#8226,#8227,#8228,#8229,#8230,#8231,#8232,#8233,#8234,#8235,#8236,#8237,
#8238,#8239,#8240,#8241,#8242,#8243,#8244,#8245,#8246,#8247,#8248,#8249,
#8250,#8251,#8252,#8253,#8254,#8255,#8256,#8257,#8258,#8259,#8260,#8261,
#8262,#8263,#8264,#8265,#8266,#8267,#8268,#8269,#8270,#8271,#8272,#8273,
#8274,#8275,#8276,#8277,#8278,#8279,#8280,#8281,#8282,#8283,#8284,#8285,
#8286,#8287,#8288,#8289,#8290,#8291,#8292,#8293,#8294,#8295,#8296,#8297,
#8298,#8299,#8300,#8301,#8302,#8303,#8304,#8305,#8306,#8307,#8308,#8309,
#8310,#8311,#8312,#8313,#8314,#8315,#8316,#8317,#8318,#8319,#8320,#8321,
#8322,#8323,#8324,#8325,#8326,#8327,#8328,#8329,#8330,#8331,#8332,#8333,
#8334,#8335,#8336,#8337,#8338,#8339,#8340,#8341,#8342,#8343,#8344,#8345,
#8346,#8347,#8348,#8349,#8350,#8351,#8352,#8353,#8354,#8355,#8356,#8357,
#8358,#8359,#8360,#8361,#8362,#8363,#8364,#8365,#8366,#8367,#8368,#8369,
#8370,#8371,#8372,#8373,#8374,#8375,#8376,#8377,#8378,#8379,#8380,#8381,
#8382,#8383,#8384,#8385,#8386,#8387,#8388,#8389,#8390,#8391,#8392,#8393,
#8394,#8395,#8396,#8397,#8398,#8399,#8400,#8401,#8402,#8403,#8404,#8405,
#8406,#8407,#8408,#8409,#8410,#8411,#8412,#8413,#8414,#8415,#8416,#8417,
#8418,#8419,#8420,#8421,#8422,#8423,#8424,#8425,#8426,#8427,#8428,#8429,
#8430,#8431,#8432,#8433,#8434,#8435,#8436,#8437,#8438,#8439,#8440,#8441,
#8442,#8443,#8444,#8445,#8446,#8447),.UNSPECIFIED.,.F.,.F.,(4,2,2,2,2,2,
2,2,2,2,2,2,2,2,2,2,2,2,2,2,2,2,2,2,2,2,2,2,2,2,2,2,2,2,2,2,2,2,2,2,2,2,
2,2,2,2,2,2,2,2,2,2,2,2,2,2,2,2,2,2,2,2,2,2,2,2,2,2,2,2,2,2,2,2,2,2,2,2,
2,2,2,2,2,2,2,2,2,2,2,2,2,2,2,2,2,2,2,2,2,2,2,2,2,2,2,2,2,2,2,2,2,2,2,2,
2,2,2,2,2,2,2,2,2,2,2,2,2,2,2,2,2,2,2,2,2,2,2,2,2,2,2,2,2,4),(-3.4011014600555,
-3.39940690323357,-3.36821987190727,-3.30906870334161,-3.29935110609441,
-3.28807316327819,-3.27184011470122,-3.24994950733,-3.24528032609246,-3.24416062170285,
-3.2435155487649,-3.24295411679195,-3.24225412307298,-3.2411731245627,-3.23626566689753,
-3.14036220638563,-3.10216066430334,-3.09150590138587,-3.08719901143788,
-3.08499918454455,-3.08363544201015,-3.08238367081698,-3.08139290121133,
-3.08041224923559,-3.07900398090188,-3.07508859236555,-3.0112223607403,
-2.97240527940232,-2.96314717273488,-2.92404966028106,-2.92164154053198,
-2.92076268779955,-2.92017109449524,-2.91959758810996,-2.91890661572345,
-2.91718392001004,-2.90149083721128,-2.81497729793915,-2.76886105966987,
-2.7643054894577,-2.76201315710154,-2.76061070199914,-2.75932974800709,
-2.75833544147687,-2.7573656446848,-2.75599680856933,-2.75233520602908,
-2.69646612233531,-2.66685302246514,-2.60001381245473,-2.59826906781251,
-2.59749748183649,-2.59692686035156,-2.59639279454439,-2.59565192534417,
-2.59415280855494,-2.5803285603877,-2.57958608687794,-2.57754255472367,
-2.57639270456604,-2.4890183126688,-2.44548986278611,-2.44107462095199,
-2.43883439737757,-2.43745376762172,-2.43618981222795,-2.43519760947577,
-2.43422212780552,-2.43254708841092,-2.42793862720706,-2.35769359271476,
-2.33170256884607,-2.30388935359502,-2.29084594135386,-2.28117132325032,
-2.27598888088953,-2.2748308049314,-2.27417732336373,-2.27367319426155,
-2.27309750749487,-2.27200227891033,-2.26816606493582,-2.26746175827766,
-2.16447935097377,-2.13136885459105,-2.11654750944929,-2.11417242570336,
-2.11293486850434,-2.11202542158643,-2.11104418129392,-2.1093397513608,
-2.10453191919316,-2.03132658348778,-1.95700579608364,-1.95274821953981,
-1.95162232699873,-1.95096927304073,-1.95040867107091,-1.94971953446012,
-1.94839604318288,-1.94016937207797,-1.92269442738877,-1.8978763978881,
-1.821232657027,-1.81401550114089,-1.8123170311346,-1.81111419628571,-1.8094506028626,
-1.80738480834939,-1.80604608859597,-1.80401203016697,-1.80185476084991,
-1.79308955402763,-1.7911532017242,-1.78989709401582,-1.78888977685416,
-1.78774889838939,-1.78581815796213,-1.77837235200505,-1.68702556580016,
-1.64335131533585,-1.64298019569692,-1.64206622556867,-1.63038694086426,
-1.62881908297876,-1.62807735792684,-1.62752258343268,-1.62701725393456,
-1.62616202898285,-1.62517961730373,-1.62340473675258,-1.60908957788495,
-1.59123682585296,-1.47526132780508,-1.46924213718703,-1.46737582758715,
-1.46636209971794,-1.46535724172279,-1.46413474859306,-1.46183059637055,
-1.44861454618318,-1.42730382860027,-1.38255916814419,-1.3701619549454),
 .UNSPECIFIED.);
#62=B_SPLINE_CURVE_WITH_KNOTS('',3,(#8448,#8449,#8450,#8451,#8452,#8453,
#8454,#8455,#8456,#8457,#8458,#8459,#8460,#8461,#8462,#8463,#8464,#8465,
#8466,#8467,#8468,#8469,#8470,#8471,#8472,#8473,#8474,#8475,#8476,#8477,
#8478,#8479,#8480,#8481,#8482,#8483,#8484,#8485,#8486,#8487,#8488,#8489,
#8490,#8491,#8492,#8493,#8494,#8495,#8496,#8497,#8498,#8499,#8500,#8501,
#8502,#8503,#8504,#8505,#8506,#8507,#8508,#8509,#8510,#8511,#8512,#8513,
#8514,#8515,#8516,#8517,#8518,#8519,#8520,#8521,#8522,#8523,#8524,#8525,
#8526,#8527,#8528,#8529,#8530,#8531,#8532,#8533,#8534,#8535,#8536,#8537,
#8538,#8539,#8540,#8541,#8542,#8543,#8544,#8545,#8546,#8547,#8548,#8549,
#8550,#8551,#8552,#8553,#8554,#8555,#8556,#8557,#8558,#8559,#8560,#8561,
#8562,#8563,#8564,#8565,#8566,#8567,#8568,#8569,#8570,#8571,#8572,#8573,
#8574,#8575,#8576,#8577,#8578,#8579,#8580,#8581,#8582,#8583,#8584,#8585,
#8586,#8587,#8588,#8589,#8590,#8591,#8592,#8593,#8594,#8595,#8596,#8597,
#8598,#8599,#8600,#8601,#8602,#8603,#8604,#8605,#8606,#8607,#8608,#8609,
#8610,#8611,#8612,#8613,#8614,#8615,#8616,#8617,#8618,#8619,#8620,#8621,
#8622,#8623,#8624,#8625,#8626,#8627,#8628,#8629,#8630,#8631,#8632,#8633,
#8634,#8635,#8636,#8637,#8638,#8639,#8640,#8641,#8642,#8643,#8644,#8645,
#8646,#8647,#8648,#8649,#8650,#8651,#8652,#8653,#8654,#8655,#8656,#8657,
#8658,#8659,#8660,#8661,#8662,#8663,#8664,#8665,#8666,#8667,#8668,#8669,
#8670,#8671,#8672,#8673,#8674,#8675,#8676,#8677,#8678,#8679,#8680,#8681,
#8682,#8683,#8684,#8685,#8686,#8687,#8688,#8689,#8690,#8691,#8692,#8693,
#8694,#8695,#8696,#8697,#8698,#8699,#8700,#8701,#8702,#8703,#8704,#8705,
#8706,#8707),.UNSPECIFIED.,.F.,.F.,(4,2,2,2,2,2,2,2,2,2,2,2,2,2,2,2,2,2,
2,2,2,2,2,2,2,2,2,2,2,2,2,2,2,2,2,2,2,2,2,2,2,2,2,2,2,2,2,2,2,2,2,2,2,2,
2,2,2,2,2,2,2,2,2,2,2,2,2,2,2,2,2,2,2,2,2,2,2,2,2,2,2,2,2,2,2,2,2,2,2,2,
2,2,2,2,2,2,2,2,2,2,2,2,2,2,2,2,2,2,2,2,2,2,2,2,2,2,2,2,2,2,2,2,2,2,2,2,
2,2,2,4),(-2.6920647855843,-2.66439261547396,-2.66193825728155,-2.66105299386178,
-2.66046018819521,-2.6598879651661,-2.65920135247204,-2.65756862797743,
-2.64406122980707,-2.64053004716835,-2.56143407129139,-2.5056417960861,
-2.50291085483323,-2.50071109499098,-2.49951789594537,-2.49851337085416,
-2.49749689004228,-2.49561653548507,-2.48948027174901,-2.38667307843778,
-2.34027846590777,-2.33855360027067,-2.33778574179126,-2.33721584912747,
-2.33668093742887,-2.33593656977653,-2.33401120484566,-2.30710349538859,
-2.21743524360764,-2.19279905329067,-2.17989162835144,-2.17760238305398,
-2.17638310291426,-2.17537843865337,-2.17436282065688,-2.17248698357659,
-2.1663889042745,-2.05648998007698,-2.03056475998383,-2.01699332659318,
-2.01535823770699,-2.01467111254571,-2.0140986696264,-2.01350586053559,
-2.01262100101754,-2.01017032332889,-1.96809556660331,-1.86200096319919,
-1.85585457622815,-1.85397288165234,-1.85295606383677,-1.85195144726959,
-1.85073399928539,-1.84845343997416,-1.83572390997298,-1.81091914864285,
-1.7213192650137,-1.69425360604937,-1.69232564832215,-1.69158082104481,
-1.69104576288015,-1.69047589252731,-1.68970836279523,-1.68810122419827,
-1.68592167227656,-1.66553866046491,-1.65233079280088,-1.5648096915393,
-1.53482899583954,-1.53201243250427,-1.53065067214364,-1.52968292349312,
-1.52876931186694,-1.52749990888916,-1.5250215757515,-1.50875902994798,
-1.46976995418952,-1.39929752851573,-1.37126321419471,-1.3693200759058,
-1.36857276604585,-1.36803705525047,-1.36752459514755,-1.36679288908419,
-1.36529022067289,-1.35180677557876,-1.32683745905079,-1.25789085770878,
-1.21232048863365,-1.20895036993735,-1.20762926120843,-1.2066723500484,
-1.20565187119117,-1.20429300032847,-1.20139080977996,-1.17621503570113,
-1.15530484615385,-1.09474525280727,-1.04952295291457,-1.04668888547896,
-1.04571731400844,-1.04516658429636,-1.04465953398093,-1.04396574864625,
-1.04264688189498,-1.03444003665025,-1.01706883906462,-0.951643867993534,
-0.889959209039997,-0.886170537817232,-0.884781846522835,-0.883806746443549,
-0.882895608308876,-0.881644348070232,-0.879268059234405,-0.864062309113781,
-0.82939499609107,-0.78215980211301,-0.727249928427786,-0.723878179017082,
-0.722836679154761,-0.722271860405961,-0.721767149491578,-0.721098633495444,
-0.720390907539149,-0.717514463815689,-0.71305909372594,-0.69915158303225,
-0.680503822703977,-0.661689072177721),.UNSPECIFIED.);
#63=B_SPLINE_CURVE_WITH_KNOTS('',3,(#8713,#8714,#8715,#8716,#8717,#8718,
#8719,#8720,#8721,#8722,#8723,#8724,#8725,#8726,#8727,#8728,#8729,#8730,
#8731,#8732,#8733,#8734,#8735,#8736,#8737,#8738,#8739,#8740,#8741,#8742,
#8743,#8744,#8745,#8746,#8747,#8748,#8749,#8750,#8751,#8752,#8753,#8754,
#8755,#8756,#8757,#8758,#8759,#8760,#8761,#8762,#8763,#8764,#8765,#8766,
#8767,#8768,#8769,#8770,#8771,#8772,#8773,#8774,#8775,#8776,#8777,#8778,
#8779,#8780,#8781,#8782,#8783,#8784,#8785,#8786,#8787,#8788,#8789,#8790,
#8791,#8792,#8793,#8794,#8795,#8796,#8797,#8798,#8799,#8800,#8801,#8802,
#8803,#8804,#8805,#8806,#8807,#8808,#8809,#8810,#8811,#8812,#8813,#8814,
#8815,#8816,#8817,#8818,#8819,#8820,#8821,#8822,#8823,#8824,#8825,#8826,
#8827,#8828,#8829,#8830,#8831,#8832,#8833,#8834,#8835,#8836,#8837,#8838,
#8839,#8840,#8841,#8842,#8843,#8844,#8845,#8846,#8847,#8848,#8849,#8850,
#8851,#8852,#8853,#8854,#8855,#8856,#8857,#8858,#8859,#8860,#8861,#8862,
#8863,#8864,#8865,#8866,#8867,#8868,#8869,#8870,#8871,#8872,#8873,#8874,
#8875,#8876,#8877,#8878,#8879,#8880,#8881,#8882,#8883,#8884,#8885,#8886,
#8887,#8888,#8889,#8890,#8891,#8892,#8893,#8894,#8895,#8896),
 .UNSPECIFIED.,.F.,.F.,(4,2,2,2,2,2,2,2,2,2,2,2,2,2,2,2,2,2,2,2,2,2,2,2,
2,2,2,2,2,2,2,2,2,2,2,2,2,2,2,2,2,2,2,2,2,2,2,2,2,2,2,2,2,2,2,2,2,2,2,2,
2,2,2,2,2,2,2,2,2,2,2,2,2,2,2,2,2,2,2,2,2,2,2,2,2,2,2,2,2,2,2,4),(-1.37035830239853,
-1.31313469101143,-1.28727965526401,-1.28426708703911,-1.28291822818799,
-1.28191644837135,-1.28086040695646,-1.27977354847701,-1.2782345349457,
-1.2756126501719,-1.2288193851385,-1.14860878768378,-1.14293376372204,-1.14074797571466,
-1.14047560813828,-1.13957734603937,-1.13793978753991,-1.13721267716872,
-1.12337513007256,-1.12187579809469,-1.1211349326605,-1.12060091996006,
-1.12003040419328,-1.11925904343146,-1.11751515380254,-1.05374170161686,
-0.993413216191368,-0.964378189601015,-0.961584130435153,-0.9602278372092,
-0.95926151143448,-0.958266871905048,-0.956977065171376,-0.95556234090598,
-0.953240486527951,-0.948604637073653,-0.936840576964002,-0.911121856136205,
-0.861652194387613,-0.811880750102781,-0.800279953603009,-0.798852923724145,
-0.798130299688123,-0.797601061850922,-0.797027252856783,-0.796236957908265,
-0.79438656020786,-0.744558170991191,-0.703913481258456,-0.6424904784718,
-0.638706943199471,-0.637318984531292,-0.636344039736707,-0.635351752003725,
-0.634084742226636,-0.632701647372255,-0.63045544182614,-0.62602391725306,
-0.614951456988997,-0.574360562937398,-0.481440911052703,-0.476567587938416,
-0.475489403267113,-0.474790329948266,-0.474229030039711,-0.473583432638654,
-0.472461149625609,-0.467758159441654,-0.426623297611181,-0.385670316276792,
-0.361297649963714,-0.318768890711419,-0.315443933775958,-0.31413025679984,
-0.313175136936421,-0.31217363314459,-0.310846434625592,-0.309380139520474,
-0.306934604089779,-0.301960731676674,-0.210513498715984,-0.16914182131995,
-0.166176332788331,-0.154126780661544,-0.152524337792522,-0.151787175084658,
-0.151219934211912,-0.150603296624108,-0.149610752665144,-0.146301732861082,
-0.125702996532957,-0.000961965831634676),.UNSPECIFIED.);
#64=B_SPLINE_CURVE_WITH_KNOTS('',3,(#8897,#8898,#8899,#8900,#8901,#8902,
#8903,#8904,#8905,#8906,#8907,#8908,#8909,#8910,#8911,#8912,#8913,#8914,
#8915,#8916,#8917,#8918,#8919,#8920,#8921,#8922,#8923,#8924,#8925,#8926,
#8927,#8928,#8929,#8930,#8931,#8932,#8933,#8934,#8935,#8936,#8937,#8938,
#8939,#8940,#8941,#8942,#8943,#8944,#8945,#8946,#8947,#8948,#8949,#8950,
#8951,#8952,#8953,#8954,#8955,#8956,#8957,#8958,#8959,#8960,#8961,#8962,
#8963,#8964,#8965,#8966,#8967,#8968,#8969,#8970,#8971,#8972,#8973,#8974,
#8975,#8976,#8977,#8978,#8979,#8980,#8981,#8982,#8983,#8984,#8985,#8986,
#8987,#8988,#8989,#8990,#8991,#8992,#8993,#8994,#8995,#8996,#8997,#8998,
#8999,#9000,#9001,#9002,#9003,#9004,#9005,#9006,#9007,#9008,#9009,#9010,
#9011,#9012,#9013,#9014,#9015,#9016),.UNSPECIFIED.,.F.,.F.,(4,2,2,2,2,2,
2,2,2,2,2,2,2,2,2,2,2,2,2,2,2,2,2,2,2,2,2,2,2,2,2,2,2,2,2,2,2,2,2,2,2,2,
2,2,2,2,2,2,2,2,2,2,2,2,2,2,2,2,2,4),(-4.06269744394932,-4.05769728268495,
-4.05419629673872,-4.05294702562819,-4.05196861910404,-4.0509894985384,
-4.05001337596529,-4.04833553111765,-4.04370937424276,-4.03757889468122,
-3.92938250846978,-3.914999855999,-3.89455864540268,-3.89126521792167,-3.89027431643437,
-3.88965799366881,-3.88909054528441,-3.8883524303158,-3.88674523345941,
-3.87457357768122,-3.87138149839504,-3.87039493851564,-3.86953012344522,
-3.79046894215544,-3.74926025335208,-3.73808046044618,-3.7336163870156,
-3.73135782098288,-3.72996937850653,-3.72869875596071,-3.72770560947298,
-3.72673173606717,-3.72534850187567,-3.72159730980179,-3.66086285289679,
-3.63147909661404,-3.62248639548299,-3.59378428428253,-3.57693136772514,
-3.56874615748008,-3.56742409996392,-3.56673514001948,-3.56617438810977,
-3.5655208236653,-3.56439324801888,-3.56012080636243,-3.5573491571516,-3.55584622145444,
-3.55456601528934,-3.46797793993311,-3.43119932851864,-3.41668157031755,
-3.41126043071538,-3.4086541645731,-3.40712139099913,-3.4057464346528,-3.40473662551545,
-3.40379344411166,-3.40252675287791,-3.4011014600555),.UNSPECIFIED.);
#65=B_SPLINE_CURVE_WITH_KNOTS('',3,(#9018,#9019,#9020,#9021,#9022,#9023,
#9024,#9025,#9026,#9027,#9028,#9029,#9030,#9031,#9032,#9033,#9034,#9035,
#9036,#9037,#9038,#9039,#9040,#9041,#9042,#9043,#9044,#9045,#9046,#9047,
#9048,#9049,#9050,#9051,#9052,#9053,#9054,#9055,#9056,#9057,#9058,#9059,
#9060,#9061,#9062,#9063,#9064,#9065,#9066,#9067,#9068,#9069,#9070,#9071,
#9072,#9073,#9074,#9075,#9076,#9077,#9078,#9079,#9080,#9081,#9082,#9083,
#9084,#9085,#9086,#9087,#9088,#9089,#9090,#9091,#9092,#9093,#9094,#9095,
#9096,#9097,#9098,#9099,#9100,#9101,#9102,#9103,#9104,#9105,#9106,#9107,
#9108,#9109,#9110,#9111,#9112,#9113,#9114,#9115,#9116,#9117,#9118,#9119,
#9120,#9121,#9122,#9123,#9124,#9125,#9126,#9127,#9128,#9129),
 .UNSPECIFIED.,.F.,.F.,(4,2,2,2,2,2,2,2,2,2,2,2,2,2,2,2,2,2,2,2,2,2,2,2,
2,2,2,2,2,2,2,2,2,2,2,2,2,2,2,2,2,2,2,2,2,2,2,2,2,2,2,2,2,2,2,4),(-0.661689072177721,
-0.635438189052493,-0.590996444194058,-0.58493164743744,-0.583468913200705,
-0.58224814615159,-0.580453319943521,-0.578372682005945,-0.576005193915886,
-0.57003350679353,-0.563972131075917,-0.562100578561216,-0.561085735082499,
-0.560080862959325,-0.558859928007559,-0.557564122547763,-0.552016600234222,
-0.519309604037286,-0.469724083183996,-0.410843999933654,-0.40985829866635,
-0.408088015642741,-0.401494588357825,-0.400296671927898,-0.39956884099718,
-0.399003123434441,-0.398382236902337,-0.397741810305707,-0.396798698479298,
-0.388532639403567,-0.370531405029497,-0.343430014275277,-0.318524206658404,
-0.245129471291207,-0.240599080285158,-0.238935990916333,-0.237962947212669,
-0.23705110872491,-0.235794798424088,-0.234449996398847,-0.232295025769849,
-0.215562697395506,-0.177460993323038,-0.164103860879277,-0.150549097395737,
-0.0822736035438614,-0.0781767092023072,-0.0770669934721367,-0.0764177237101079,
-0.0759129736330026,-0.0752443049929717,-0.0745363801645729,-0.0734321417212298,
-0.0713440483731208,-0.0663737342799348,-0.000961608844988501),
 .UNSPECIFIED.);
#66=B_SPLINE_CURVE_WITH_KNOTS('',3,(#9130,#9131,#9132,#9133,#9134,#9135,
#9136,#9137,#9138,#9139,#9140,#9141,#9142,#9143,#9144,#9145,#9146,#9147,
#9148,#9149,#9150,#9151,#9152,#9153,#9154,#9155,#9156,#9157,#9158,#9159,
#9160,#9161,#9162,#9163,#9164,#9165,#9166,#9167,#9168,#9169,#9170,#9171,
#9172,#9173,#9174,#9175,#9176,#9177,#9178,#9179,#9180,#9181,#9182,#9183,
#9184,#9185,#9186,#9187,#9188,#9189,#9190,#9191,#9192,#9193,#9194,#9195,
#9196,#9197,#9198,#9199,#9200,#9201,#9202,#9203,#9204,#9205,#9206,#9207,
#9208,#9209,#9210,#9211,#9212,#9213,#9214,#9215,#9216,#9217,#9218,#9219,
#9220,#9221,#9222,#9223,#9224,#9225,#9226,#9227,#9228,#9229,#9230,#9231,
#9232,#9233,#9234,#9235,#9236,#9237,#9238,#9239,#9240,#9241,#9242,#9243,
#9244,#9245,#9246,#9247,#9248,#9249,#9250,#9251,#9252,#9253,#9254,#9255,
#9256,#9257,#9258,#9259,#9260,#9261,#9262,#9263,#9264,#9265,#9266,#9267,
#9268,#9269,#9270,#9271,#9272,#9273,#9274,#9275,#9276,#9277,#9278,#9279,
#9280,#9281,#9282,#9283,#9284,#9285,#9286,#9287,#9288,#9289,#9290,#9291,
#9292,#9293,#9294,#9295,#9296,#9297,#9298,#9299,#9300,#9301,#9302,#9303,
#9304,#9305,#9306,#9307,#9308,#9309,#9310,#9311,#9312,#9313,#9314,#9315),
 .UNSPECIFIED.,.F.,.F.,(4,2,2,2,2,2,2,2,2,2,2,2,2,2,2,2,2,2,2,2,2,2,2,2,
2,2,2,2,2,2,2,2,2,2,2,2,2,2,2,2,2,2,2,2,2,2,2,2,2,2,2,2,2,2,2,2,2,2,2,2,
2,2,2,2,2,2,2,2,2,2,2,2,2,2,2,2,2,2,2,2,2,2,2,2,2,2,2,2,2,2,2,2,4),(-4.06100209435087,
-3.99455560708784,-3.9799802658478,-3.97790988131639,-3.97660085526456,
-3.97537049774392,-3.97446220133678,-3.97347818791015,-3.97175853731164,
-3.96684176792589,-3.8898848744918,-3.87632607302362,-3.86335695204296,
-3.82964209247129,-3.81598622941117,-3.81491794097997,-3.81422522916569,
-3.81356751272227,-3.81306352537448,-3.81249163710651,-3.81141437192997,
-3.80773615102716,-3.74489621682546,-3.72512656377337,-3.70572059584182,
-3.67134460217803,-3.66137806910723,-3.65518898642008,-3.65384984143269,
-3.65259772176189,-3.6516867355372,-3.65071253387599,-3.64904230119304,
-3.64446232015115,-3.57072446860636,-3.52360757989629,-3.49393137331868,
-3.49187666891556,-3.49124009192201,-3.49062194848218,-3.49005570650699,
-3.48932309362008,-3.48774316428525,-3.47625840010405,-3.42646231826365,
-3.37883915944638,-3.34767087233704,-3.3382353631171,-3.33230296159233,
-3.33098072401437,-3.3297408039214,-3.3288313216303,-3.32785167709853,-3.3264458286726,
-3.32254334017667,-3.26199759757763,-3.22016726552227,-3.17084226879795,
-3.16898847479866,-3.16818886319945,-3.1676135052689,-3.16708660809439,
-3.16637263726346,-3.16497889110281,-3.15427841300663,-3.1117435476327,
-3.04871541558155,-3.035863543586,-3.01149295543485,-3.00852050467562,-3.0071495207056,
-3.00612731388847,-3.00517410550499,-3.00386643315513,-3.00057430202474,
-2.95990623994496,-2.90573108384631,-2.84868236481933,-2.84633542609704,
-2.84545874198934,-2.84486782798132,-2.84429435542709,-2.84360270342334,
-2.84187453489065,-2.82596590609577,-2.82516723917376,-2.82398244416466,
-2.82283234395509,-2.81810332315078,-2.80653581748999,-2.74224851330479,
-2.71809003659731,-2.6925136763791),.UNSPECIFIED.);
#67=B_SPLINE_CURVE_WITH_KNOTS('',3,(#9320,#9321,#9322,#9323,#9324,#9325,
#9326,#9327,#9328,#9329,#9330,#9331,#9332,#9333,#9334,#9335,#9336,#9337,
#9338,#9339,#9340,#9341,#9342,#9343,#9344,#9345,#9346,#9347,#9348,#9349,
#9350,#9351,#9352,#9353,#9354,#9355,#9356,#9357,#9358,#9359,#9360,#9361,
#9362,#9363,#9364,#9365,#9366,#9367,#9368,#9369,#9370,#9371,#9372,#9373,
#9374,#9375,#9376,#9377,#9378,#9379,#9380,#9381,#9382,#9383,#9384,#9385,
#9386,#9387,#9388,#9389,#9390,#9391,#9392,#9393,#9394,#9395,#9396,#9397,
#9398,#9399,#9400,#9401,#9402,#9403,#9404,#9405,#9406,#9407,#9408,#9409,
#9410,#9411,#9412,#9413,#9414,#9415,#9416,#9417,#9418,#9419,#9420,#9421,
#9422,#9423,#9424,#9425,#9426,#9427,#9428,#9429,#9430,#9431,#9432,#9433,
#9434,#9435,#9436,#9437,#9438,#9439,#9440,#9441,#9442,#9443,#9444,#9445,
#9446,#9447,#9448,#9449,#9450,#9451,#9452,#9453,#9454,#9455,#9456,#9457,
#9458,#9459,#9460,#9461,#9462,#9463,#9464,#9465,#9466,#9467,#9468,#9469,
#9470,#9471,#9472,#9473,#9474,#9475,#9476,#9477,#9478,#9479,#9480,#9481,
#9482,#9483,#9484,#9485,#9486,#9487,#9488,#9489,#9490,#9491,#9492,#9493,
#9494,#9495,#9496,#9497,#9498,#9499,#9500,#9501,#9502,#9503,#9504,#9505,
#9506,#9507,#9508,#9509,#9510,#9511,#9512,#9513,#9514,#9515,#9516,#9517,
#9518,#9519,#9520,#9521,#9522,#9523,#9524,#9525,#9526,#9527,#9528,#9529,
#9530,#9531,#9532,#9533,#9534,#9535,#9536,#9537,#9538,#9539,#9540,#9541,
#9542,#9543,#9544,#9545,#9546,#9547,#9548,#9549,#9550,#9551,#9552,#9553,
#9554,#9555,#9556,#9557,#9558,#9559,#9560,#9561,#9562,#9563,#9564,#9565,
#9566,#9567,#9568,#9569,#9570,#9571,#9572,#9573,#9574,#9575,#9576,#9577,
#9578,#9579,#9580,#9581,#9582,#9583,#9584,#9585,#9586,#9587,#9588,#9589,
#9590,#9591,#9592,#9593,#9594,#9595,#9596,#9597,#9598,#9599,#9600,#9601,
#9602,#9603,#9604,#9605,#9606,#9607,#9608,#9609,#9610,#9611,#9612,#9613,
#9614,#9615,#9616,#9617,#9618,#9619),.UNSPECIFIED.,.F.,.F.,(4,2,2,2,2,2,
2,2,2,2,2,2,2,2,2,2,2,2,2,2,2,2,2,2,2,2,2,2,2,2,2,2,2,2,2,2,2,2,2,2,2,2,
2,2,2,2,2,2,2,2,2,2,2,2,2,2,2,2,2,2,2,2,2,2,2,2,2,2,2,2,2,2,2,2,2,2,2,2,
2,2,2,2,2,2,2,2,2,2,2,2,2,2,2,2,2,2,2,2,2,2,2,2,2,2,2,2,2,2,2,2,2,2,2,2,
2,2,2,2,2,2,2,2,2,2,2,2,2,2,2,2,2,2,2,2,2,2,2,2,2,2,2,2,2,2,2,2,2,2,2,4),
(-3.39999468752269,-3.39888508074895,-3.38864706455002,-3.38509663653904,
-3.38268746164111,-3.38181149302039,-3.38128715723683,-3.38071938172533,
-3.37997472378146,-3.3783895199414,-3.36620885509757,-3.36431102179285,
-3.36350557505008,-3.36066389792965,-3.35826263009743,-3.28322487147196,
-3.27240876426585,-3.25782147723038,-3.23721101923308,-3.22399249708449,
-3.22168999736582,-3.22046862673111,-3.21946481876955,-3.21845225744448,
-3.21658840847785,-3.21057959252479,-3.09478492549836,-3.07038515236454,
-3.06397606651343,-3.06145808168865,-3.06019301332519,-3.05917426282592,
-3.05854171868414,-3.05798110276021,-3.05728378940053,-3.05620999191957,
-3.05138190052675,-3.04960353058936,-2.95023621548289,-2.92055330625379,
-2.91441984394696,-2.90100967030443,-2.89869793968004,-2.89747449778693,
-2.89647044774759,-2.89545887927529,-2.89360042141055,-2.88763692976508,
-2.77233105442108,-2.73876116446253,-2.73735042193173,-2.73651509781933,
-2.73578906201379,-2.73522736804566,-2.73469843432204,-2.73397595410638,
-2.73254839467543,-2.72090997493493,-2.68617234992351,-2.6422701669739,
-2.58203916238946,-2.57692658816435,-2.57524317301434,-2.57415807470247,
-2.57313731475397,-2.57179671244384,-2.56953289705597,-2.56112848814692,
-2.55874935774861,-2.55747416869619,-2.55643606692916,-2.55434453136443,
-2.5524633351361,-2.55123620156271,-2.54953914460951,-2.54330753556182,
-2.53550203470692,-2.51802674103955,-2.44612949765603,-2.4383487614759,
-2.41763880761357,-2.41543956523201,-2.41429325959219,-2.41356785869525,
-2.41293267031608,-2.41238213272442,-2.41182567081232,-2.41082439908466,
-2.40776673548098,-2.35821704159072,-2.33281474312137,-2.30729793574649,
-2.27115952245672,-2.2555488883302,-2.25314360446534,-2.25190019672765,
-2.25089456907919,-2.24989370347248,-2.24808939695326,-2.24255523589577,
-2.12307154915067,-2.10104919731347,-2.09198834659389,-2.09063259873344,
-2.08993690514599,-2.08937614274246,-2.08881277172444,-2.08777782748419,
-2.0844578196934,-2.03185402404902,-1.96193156576471,-1.93351498386433,
-1.93042826785742,-1.92918895701729,-1.92815930181385,-1.92710701207653,
-1.92557727089689,-1.92157658895362,-1.8687140264278,-1.77366811607669,
-1.76873953027171,-1.76765722655489,-1.76695702573442,-1.76639585391538,
-1.76575155236312,-1.76463435124635,-1.75999152737085,-1.73561832620679,
-1.68788408213307,-1.61284999384229,-1.60813010439633,-1.60643876948035,
-1.60546029039319,-1.60447009905361,-1.60321326545907,-1.60184409976123,
-1.59963082210951,-1.59528713057083,-1.55299102686655,-1.45000802481392,
-1.44929931922799,-1.44546650164039,-1.4443717360424,-1.44379618910936,
-1.44329212511127,-1.44263864881901,-1.44148035732081,-1.43629338899788,
-1.38259972603757,-1.37035830239853),.UNSPECIFIED.);
#68=B_SPLINE_CURVE_WITH_KNOTS('',3,(#9620,#9621,#9622,#9623,#9624,#9625,
#9626,#9627,#9628,#9629,#9630,#9631,#9632,#9633,#9634,#9635,#9636,#9637,
#9638,#9639,#9640,#9641,#9642,#9643,#9644,#9645,#9646,#9647,#9648,#9649,
#9650,#9651,#9652,#9653,#9654,#9655,#9656,#9657,#9658,#9659,#9660,#9661,
#9662,#9663,#9664,#9665,#9666,#9667,#9668,#9669,#9670,#9671,#9672,#9673,
#9674,#9675,#9676,#9677,#9678,#9679,#9680,#9681,#9682,#9683,#9684,#9685,
#9686,#9687,#9688,#9689,#9690,#9691,#9692,#9693,#9694,#9695,#9696,#9697,
#9698,#9699,#9700,#9701,#9702,#9703,#9704,#9705,#9706,#9707,#9708,#9709,
#9710,#9711,#9712,#9713,#9714,#9715,#9716,#9717,#9718,#9719,#9720,#9721,
#9722,#9723,#9724,#9725,#9726,#9727,#9728,#9729,#9730,#9731,#9732,#9733,
#9734,#9735,#9736,#9737,#9738,#9739,#9740,#9741,#9742,#9743,#9744,#9745,
#9746,#9747,#9748,#9749,#9750,#9751,#9752,#9753,#9754,#9755,#9756,#9757,
#9758,#9759,#9760,#9761,#9762,#9763,#9764,#9765,#9766,#9767,#9768,#9769,
#9770,#9771,#9772,#9773,#9774,#9775,#9776,#9777,#9778,#9779,#9780,#9781,
#9782,#9783,#9784,#9785,#9786,#9787,#9788,#9789,#9790,#9791,#9792,#9793,
#9794,#9795,#9796,#9797,#9798,#9799,#9800,#9801,#9802,#9803,#9804,#9805,
#9806,#9807,#9808,#9809,#9810,#9811,#9812,#9813,#9814,#9815,#9816,#9817,
#9818,#9819,#9820,#9821,#9822,#9823,#9824,#9825,#9826,#9827,#9828,#9829,
#9830,#9831,#9832,#9833,#9834,#9835,#9836,#9837,#9838,#9839,#9840,#9841,
#9842,#9843,#9844,#9845,#9846,#9847,#9848,#9849,#9850,#9851,#9852,#9853,
#9854,#9855,#9856,#9857,#9858,#9859,#9860,#9861,#9862,#9863,#9864,#9865,
#9866,#9867,#9868,#9869,#9870,#9871,#9872,#9873,#9874,#9875,#9876,#9877,
#9878,#9879,#9880,#9881,#9882,#9883,#9884,#9885,#9886,#9887,#9888,#9889,
#9890,#9891,#9892,#9893,#9894,#9895,#9896,#9897),.UNSPECIFIED.,.F.,.F.,
(4,2,2,2,2,2,2,2,2,2,2,2,2,2,2,2,2,2,2,2,2,2,2,2,2,2,2,2,2,2,2,2,2,2,2,
2,2,2,2,2,2,2,2,2,2,2,2,2,2,2,2,2,2,2,2,2,2,2,2,2,2,2,2,2,2,2,2,2,2,2,2,
2,2,2,2,2,2,2,2,2,2,2,2,2,2,2,2,2,2,2,2,2,2,2,2,2,2,2,2,2,2,2,2,2,2,2,2,
2,2,2,2,2,2,2,2,2,2,2,2,2,2,2,2,2,2,2,2,2,2,2,2,2,2,2,2,2,2,2,4),(-2.6925136763791,
-2.691349806873,-2.68640116471688,-2.6847420978949,-2.68365459336578,-2.68263420918073,
-2.68129791328207,-2.67835241356829,-2.65458726286017,-2.57907715134864,
-2.52685699631286,-2.52369001010775,-2.52271639452321,-2.5220997531916,
-2.52153294171388,-2.52079693011943,-2.51919931032582,-2.50726036352065,
-2.50504097216832,-2.5045954377761,-2.50143518369202,-2.49992602349204,
-2.49005744146085,-2.40221200913805,-2.36925639200468,-2.36361340174826,
-2.36186981615955,-2.36076313081419,-2.3597493959125,-2.35845602235567,
-2.35573665319751,-2.33780810447716,-2.23833461440736,-2.20212271255252,
-2.20022827525242,-2.19943044815193,-2.19885534515629,-2.19832793751886,
-2.19761220027943,-2.19621182765393,-2.18534109143103,-2.09464422253666,
-2.06218172455028,-2.04193918166971,-2.03938353835468,-2.03810881243561,
-2.03719455235325,-2.03622905099406,-2.03487522894154,-2.03130487181021,
-1.97577546092888,-1.88285738028345,-1.87796215404449,-1.87688239824507,
-1.87618293235685,-1.8756217371776,-1.8749767271081,-1.87385661720462,-1.86917864839645,
-1.84850855819866,-1.82401713854521,-1.72446273836435,-1.71775253061962,
-1.71580567719067,-1.71466137512114,-1.7136643584933,-1.71241861201454,
-1.71000381108026,-1.69446940103456,-1.65855407987267,-1.56117872848709,
-1.56005999373534,-1.55536844185267,-1.55398410911901,-1.55327244697552,
-1.5527460198217,-1.55216990393184,-1.55138317673594,-1.54954048025857,
-1.54700661574797,-1.45836767630944,-1.39757116530015,-1.39378758417087,
-1.39239971367785,-1.39142486356331,-1.3905136993963,-1.38926200027535,
-1.38681901008649,-1.37053883454821,-1.33180691023247,-1.25892054890241,
-1.2329218234999,-1.23101122226387,-1.23026929813183,-1.22973502606504,
-1.22916472525219,-1.22840998355347,-1.22673891589629,-1.22449778758587,
-1.20312610057062,-1.14465354267821,-1.07538637235953,-1.07102003655398,
-1.06938228554458,-1.06841426881729,-1.06750074604691,-1.06623200970819,
-1.06370643325601,-1.04487226252374,-1.01612719711402,-0.951140483009,-0.928195914060588,
-0.923765851911744,-0.92344539762017,-0.922559001780413,-0.92206110623185,
-0.921239750865158,-0.909445831829231,-0.908012143660318,-0.907287848318172,
-0.906758201819078,-0.906184771704657,-0.905616981718027,-0.904234372019432,
-0.894275702962061,-0.868548219656582,-0.824502336248255,-0.786177246901088,
-0.750861781069498,-0.747670596246262,-0.746380038215635,-0.7454310422672,
-0.744405458233358,-0.743016065842197,-0.739862866114819,-0.735647400735218,
-0.72529396470047,-0.688761199217399,-0.662310186026634),.UNSPECIFIED.);
#69=B_SPLINE_CURVE_WITH_KNOTS('',3,(#9903,#9904,#9905,#9906,#9907,#9908,
#9909,#9910,#9911,#9912,#9913,#9914,#9915,#9916,#9917,#9918,#9919,#9920,
#9921,#9922,#9923,#9924,#9925,#9926,#9927,#9928,#9929,#9930,#9931,#9932,
#9933,#9934,#9935,#9936,#9937,#9938,#9939,#9940,#9941,#9942,#9943,#9944,
#9945,#9946,#9947,#9948,#9949,#9950,#9951,#9952,#9953,#9954,#9955,#9956,
#9957,#9958,#9959,#9960,#9961,#9962,#9963,#9964,#9965,#9966,#9967,#9968,
#9969,#9970,#9971,#9972,#9973,#9974,#9975,#9976,#9977,#9978,#9979,#9980,
#9981,#9982,#9983,#9984,#9985,#9986,#9987,#9988,#9989,#9990,#9991,#9992,
#9993,#9994,#9995,#9996,#9997,#9998,#9999,#10000,#10001,#10002,#10003,#10004,
#10005,#10006,#10007,#10008,#10009,#10010,#10011,#10012,#10013,#10014,#10015,
#10016,#10017,#10018,#10019,#10020,#10021,#10022,#10023,#10024,#10025,#10026,
#10027,#10028,#10029,#10030,#10031,#10032,#10033,#10034,#10035,#10036,#10037,
#10038,#10039,#10040,#10041,#10042,#10043,#10044,#10045,#10046,#10047,#10048,
#10049,#10050,#10051,#10052,#10053,#10054,#10055,#10056,#10057,#10058,#10059,
#10060,#10061,#10062,#10063,#10064,#10065,#10066,#10067,#10068,#10069,#10070,
#10071,#10072,#10073,#10074,#10075,#10076,#10077,#10078,#10079,#10080,#10081,
#10082,#10083,#10084,#10085,#10086,#10087,#10088,#10089,#10090,#10091,#10092,
#10093,#10094,#10095,#10096,#10097,#10098,#10099,#10100,#10101,#10102,#10103,
#10104),.UNSPECIFIED.,.F.,.F.,(4,2,2,2,2,2,2,2,2,2,2,2,2,2,2,2,2,2,2,2,
2,2,2,2,2,2,2,2,2,2,2,2,2,2,2,2,2,2,2,2,2,2,2,2,2,2,2,2,2,2,2,2,2,2,2,2,
2,2,2,2,2,2,2,2,2,2,2,2,2,2,2,2,2,2,2,2,2,2,2,2,2,2,2,2,2,2,2,2,2,2,2,2,
2,2,2,2,2,2,2,2,4),(-1.3702925990382,-1.3646065123406,-1.27381134544931,
-1.26205774028186,-1.26048731237941,-1.25974516762392,-1.25917732763983,
-1.2585757189674,-1.25762589165693,-1.25650806933852,-1.25438432904009,
-1.20624500881719,-1.12921162168623,-1.12272149643121,-1.12122673262677,
-1.12003174308615,-1.11602423209939,-1.11530461207618,-1.11455244310793,
-1.11259160846636,-1.1105820478428,-1.10240224398722,-1.09984033023852,
-1.09854647352297,-1.09753532305077,-1.09641744438754,-1.09458889816991,
-1.08820716803191,-1.04822639192728,-0.94698832566313,-0.944720812359825,
-0.939614549818961,-0.937602984484482,-0.936844557767111,-0.93630582110514,
-0.935765248411139,-0.935040869744138,-0.933530231521145,-0.931550960094603,
-0.926928277091865,-0.912352090239843,-0.86819304746328,-0.783333380593811,
-0.777841309673415,-0.776041777992556,-0.775041428159509,-0.774044511468714,
-0.772802473239471,-0.770406213141967,-0.755060245452764,-0.719928202648477,
-0.680221302447579,-0.627071353120496,-0.615888049739316,-0.614339582183063,
-0.613601817153927,-0.613034613347241,-0.612430946893631,-0.611472420612584,
-0.608449013701643,-0.603696300615647,-0.588628875062841,-0.558037195675566,
-0.480775846255374,-0.477210432570438,-0.456630396520522,-0.453799586835005,
-0.452484579458253,-0.451467380005995,-0.450370380424853,-0.448635643767317,
-0.443107075048842,-0.411414326406116,-0.364605389980612,-0.343762929276641,
-0.315764345385161,-0.304771280431548,-0.292978694522289,-0.291545053713341,
-0.290820771269963,-0.290291128937723,-0.289756696103606,-0.289196703169409,
-0.287886894078347,-0.279897516335745,-0.269422982829613,-0.250014896693966,
-0.159080377076261,-0.152993827463823,-0.151575859332063,-0.150360477391903,
-0.149235963728482,-0.133323365037272,-0.130698876511579,-0.129410171985675,
-0.128399637948359,-0.12727894164361,-0.125437813426122,-0.118933080236084,
-0.0776491223565139,-0.000962580391007859),.UNSPECIFIED.);
#70=B_SPLINE_CURVE_WITH_KNOTS('',3,(#10105,#10106,#10107,#10108,#10109,
#10110,#10111,#10112,#10113,#10114,#10115,#10116,#10117,#10118,#10119,#10120,
#10121,#10122,#10123,#10124,#10125,#10126,#10127,#10128,#10129,#10130,#10131,
#10132,#10133,#10134,#10135,#10136,#10137,#10138,#10139,#10140,#10141,#10142,
#10143,#10144,#10145,#10146,#10147,#10148,#10149,#10150,#10151,#10152,#10153,
#10154,#10155,#10156,#10157,#10158,#10159,#10160,#10161,#10162,#10163,#10164,
#10165,#10166,#10167,#10168,#10169,#10170,#10171,#10172,#10173,#10174,#10175,
#10176,#10177,#10178,#10179,#10180,#10181,#10182,#10183,#10184,#10185,#10186,
#10187,#10188,#10189,#10190,#10191,#10192,#10193,#10194,#10195,#10196,#10197,
#10198,#10199,#10200,#10201,#10202,#10203,#10204,#10205,#10206,#10207,#10208),
 .UNSPECIFIED.,.F.,.F.,(4,2,2,2,2,2,2,2,2,2,2,2,2,2,2,2,2,2,2,2,2,2,2,2,
2,2,2,2,2,2,2,2,2,2,2,2,2,2,2,2,2,2,2,2,2,2,2,2,2,2,2,4),(-4.06022502783442,
-4.02941315715002,-4.02823287730869,-4.02749340286536,-4.02693407807125,
-4.02640041630651,-4.02587157338326,-4.02514859807187,-4.02371819358163,
-4.01197934923213,-4.00949075323713,-4.0064615868957,-4.00521260221354,
-3.99508509257341,-3.99114949833664,-3.90677322024206,-3.8821592639454,
-3.86927324002438,-3.86698720772121,-3.86576956874246,-3.86486342118252,
-3.86373134735246,-3.86183522300634,-3.85555453413604,-3.74871266922852,
-3.72825477858468,-3.71320185323394,-3.70601251083289,-3.70474081534874,
-3.70418537588386,-3.70364868783383,-3.70311530088758,-3.70237512240616,
-3.70047179238169,-3.67479848416132,-3.63234380886613,-3.62733850302291,
-3.6215698809821,-3.6148179562441,-3.60673143078635,-3.59666542673705,-3.56642698230218,
-3.54702559194131,-3.54449541904677,-3.54322663484052,-3.54231396997977,
-3.54134768856648,-3.53998875073913,-3.53718047533541,-3.50744583280931,
-3.41987959723944,-3.39999468752269),.UNSPECIFIED.);
#71=B_SPLINE_CURVE_WITH_KNOTS('',3,(#10210,#10211,#10212,#10213,#10214,
#10215,#10216,#10217,#10218,#10219,#10220,#10221,#10222,#10223,#10224,#10225,
#10226,#10227,#10228,#10229,#10230,#10231,#10232,#10233,#10234,#10235,#10236,
#10237,#10238,#10239,#10240,#10241,#10242,#10243,#10244,#10245,#10246,#10247,
#10248,#10249,#10250,#10251,#10252,#10253,#10254,#10255,#10256,#10257,#10258,
#10259,#10260,#10261,#10262,#10263,#10264,#10265,#10266,#10267,#10268,#10269,
#10270,#10271,#10272,#10273,#10274,#10275,#10276,#10277,#10278,#10279,#10280,
#10281,#10282,#10283,#10284,#10285,#10286,#10287,#10288,#10289,#10290,#10291,
#10292,#10293,#10294,#10295,#10296,#10297,#10298,#10299,#10300,#10301,#10302,
#10303,#10304,#10305),.UNSPECIFIED.,.F.,.F.,(4,2,2,2,2,2,2,2,2,2,2,2,2,
2,2,2,2,2,2,2,2,2,2,2,2,2,2,2,2,2,2,2,2,2,2,2,2,2,2,2,2,2,2,2,2,2,2,4),
(-0.662310186026634,-0.63675288603753,-0.588333427674046,-0.585495917556745,
-0.584523823481245,-0.583972982986467,-0.583465948922825,-0.582926218405347,
-0.582247573747971,-0.579734924363326,-0.554581793756154,-0.513735407137791,
-0.430827978459099,-0.42545535422149,-0.423671792629946,-0.422674708205422,
-0.421677361040954,-0.420429282494195,-0.418003824836794,-0.402185690190519,
-0.365209064224272,-0.341759075045079,-0.318182644017952,-0.272511262305969,
-0.271630528862389,-0.269488261566253,-0.268791595284995,-0.263087101133857,
-0.261947064187762,-0.261228984229397,-0.260666055906529,-0.260033283919376,
-0.259375842766903,-0.258391869657778,-0.248318115196362,-0.218297281671593,
-0.196686020435488,-0.164401118176624,-0.105937940264548,-0.102102229561359,
-0.100706312914663,-0.0997292351256157,-0.0988186995731407,-0.0975720540397754,
-0.0951534505095346,-0.0921177860775552,-0.0854576127161563,-0.000962002473629624),
 .UNSPECIFIED.);
#72=B_SPLINE_CURVE_WITH_KNOTS('',3,(#10306,#10307,#10308,#10309,#10310,
#10311,#10312,#10313,#10314,#10315,#10316,#10317,#10318,#10319,#10320,#10321,
#10322,#10323,#10324,#10325,#10326,#10327,#10328,#10329,#10330,#10331,#10332,
#10333,#10334,#10335,#10336,#10337,#10338,#10339,#10340,#10341,#10342,#10343,
#10344,#10345,#10346,#10347,#10348,#10349,#10350,#10351,#10352,#10353,#10354,
#10355,#10356,#10357,#10358,#10359,#10360,#10361,#10362,#10363,#10364,#10365,
#10366,#10367,#10368,#10369,#10370,#10371,#10372,#10373,#10374,#10375,#10376,
#10377,#10378,#10379,#10380,#10381,#10382,#10383,#10384,#10385,#10386,#10387,
#10388,#10389,#10390,#10391,#10392,#10393,#10394,#10395,#10396,#10397,#10398,
#10399,#10400,#10401,#10402,#10403,#10404,#10405,#10406,#10407,#10408,#10409,
#10410,#10411,#10412,#10413,#10414,#10415,#10416,#10417,#10418,#10419,#10420,
#10421,#10422,#10423,#10424,#10425,#10426,#10427,#10428,#10429,#10430,#10431,
#10432,#10433,#10434,#10435,#10436,#10437,#10438,#10439,#10440,#10441,#10442,
#10443,#10444,#10445,#10446,#10447,#10448,#10449,#10450,#10451,#10452,#10453,
#10454,#10455,#10456,#10457,#10458,#10459,#10460,#10461,#10462,#10463,#10464,
#10465,#10466,#10467,#10468,#10469,#10470,#10471,#10472,#10473,#10474,#10475,
#10476,#10477,#10478,#10479,#10480,#10481,#10482,#10483,#10484,#10485,#10486,
#10487,#10488,#10489,#10490,#10491,#10492,#10493,#10494,#10495,#10496,#10497,
#10498,#10499,#10500,#10501,#10502,#10503,#10504,#10505,#10506,#10507,#10508,
#10509,#10510,#10511,#10512,#10513),.UNSPECIFIED.,.F.,.F.,(4,2,2,2,2,2,
2,2,2,2,2,2,2,2,2,2,2,2,2,2,2,2,2,2,2,2,2,2,2,2,2,2,2,2,2,2,2,2,2,2,2,2,
2,2,2,2,2,2,2,2,2,2,2,2,2,2,2,2,2,2,2,2,2,2,2,2,2,2,2,2,2,2,2,2,2,2,2,2,
2,2,2,2,2,2,2,2,2,2,2,2,2,2,2,2,2,2,2,2,2,2,2,2,2,4),(-4.06056306224649,
-4.00985058969614,-4.00047566401566,-3.99927624979501,-3.99852851797568,
-3.99796591941104,-3.99739545221306,-3.99686196455536,-3.99612255299507,
-3.99462843663741,-3.98095180342464,-3.93541206834487,-3.92650036975616,
-3.91864565346336,-3.90263572260438,-3.85548687998933,-3.84042440568608,
-3.83801353337325,-3.83676872045931,-3.83577191818468,-3.83477364763648,
-3.83298324221768,-3.82755697749892,-3.74384889337152,-3.72134051564925,
-3.69445809408888,-3.68274511411716,-3.67882574084003,-3.67622341349027,
-3.67553726710497,-3.67499540862029,-3.67443926633666,-3.6738805548619,
-3.67286882114242,-3.66973286857439,-3.61554262387277,-3.56900443110658,
-3.5615389306865,-3.53162004954608,-3.51746577710315,-3.5151073368869,-3.51387348504589,
-3.51296468059732,-3.51198212267652,-3.5105658689147,-3.50659468729772,
-3.50525807506071,-3.42574751033429,-3.37579235840384,-3.36107607754459,
-3.35402005146516,-3.35275377957752,-3.35207139440789,-3.35156565972193,
-3.35100929345434,-3.35000930641327,-3.34696359670673,-3.29818937034096,
-3.22980483856678,-3.21024608269278,-3.19475618838003,-3.19226724864279,
-3.19100618385251,-3.19009389309821,-3.18912317551664,-3.18775003749894,
-3.18405936842057,-3.12813059961869,-3.08586260021177,-3.05379676072633,
-3.03848417538124,-3.03366158559336,-3.03060479226204,-3.02964209897921,
-3.02902795844688,-3.02846032211443,-3.02771892548804,-3.02615182056934,
-3.01448024757926,-2.99043663390157,-2.98859997049405,-2.92422629668604,
-2.90054553349135,-2.87289571018539,-2.86980768386537,-2.86841422289142,
-2.86738814031535,-2.86644045265128,-2.86515437796379,-2.86263875821785,
-2.8429386004191,-2.83537413996105,-2.81050277336572,-2.74989750382703,
-2.72666473447658,-2.71056167749424,-2.70866304294895,-2.70720333005324,
-2.70648887007284,-2.70597692831379,-2.70544057491816,-2.70469054667675,
-2.70272995443796,-2.69255696121762),.UNSPECIFIED.);
#73=B_SPLINE_CURVE_WITH_KNOTS('',3,(#10518,#10519,#10520,#10521,#10522,
#10523,#10524,#10525,#10526,#10527,#10528,#10529,#10530,#10531,#10532,#10533,
#10534,#10535,#10536,#10537,#10538,#10539,#10540,#10541,#10542,#10543,#10544,
#10545,#10546,#10547,#10548,#10549,#10550,#10551,#10552,#10553,#10554,#10555,
#10556,#10557,#10558,#10559,#10560,#10561,#10562,#10563,#10564,#10565,#10566,
#10567,#10568,#10569,#10570,#10571,#10572,#10573,#10574,#10575,#10576,#10577,
#10578,#10579,#10580,#10581,#10582,#10583,#10584,#10585,#10586,#10587,#10588,
#10589,#10590,#10591,#10592,#10593,#10594,#10595,#10596,#10597,#10598,#10599,
#10600,#10601,#10602,#10603,#10604,#10605,#10606,#10607,#10608,#10609,#10610,
#10611,#10612,#10613,#10614,#10615,#10616,#10617,#10618,#10619,#10620,#10621,
#10622,#10623,#10624,#10625,#10626,#10627,#10628,#10629,#10630,#10631,#10632,
#10633,#10634,#10635,#10636,#10637,#10638,#10639,#10640,#10641,#10642,#10643,
#10644,#10645,#10646,#10647,#10648,#10649,#10650,#10651,#10652,#10653,#10654,
#10655,#10656,#10657,#10658,#10659,#10660,#10661,#10662,#10663,#10664,#10665,
#10666,#10667,#10668,#10669,#10670,#10671,#10672,#10673,#10674,#10675,#10676,
#10677,#10678,#10679,#10680,#10681,#10682,#10683,#10684,#10685,#10686,#10687,
#10688,#10689,#10690,#10691,#10692,#10693,#10694,#10695,#10696,#10697,#10698,
#10699,#10700,#10701,#10702,#10703,#10704,#10705,#10706,#10707,#10708,#10709,
#10710,#10711,#10712,#10713,#10714,#10715,#10716,#10717,#10718,#10719,#10720,
#10721,#10722,#10723,#10724,#10725,#10726,#10727,#10728,#10729,#10730,#10731,
#10732,#10733,#10734,#10735,#10736,#10737,#10738,#10739,#10740,#10741,#10742,
#10743,#10744,#10745,#10746,#10747,#10748,#10749,#10750,#10751,#10752,#10753,
#10754,#10755,#10756,#10757,#10758,#10759,#10760,#10761,#10762,#10763,#10764,
#10765,#10766,#10767,#10768,#10769,#10770,#10771,#10772,#10773,#10774,#10775,
#10776,#10777,#10778,#10779,#10780,#10781,#10782,#10783,#10784,#10785),
 .UNSPECIFIED.,.F.,.F.,(4,2,2,2,2,2,2,2,2,2,2,2,2,2,2,2,2,2,2,2,2,2,2,2,
2,2,2,2,2,2,2,2,2,2,2,2,2,2,2,2,2,2,2,2,2,2,2,2,2,2,2,2,2,2,2,2,2,2,2,2,
2,2,2,2,2,2,2,2,2,2,2,2,2,2,2,2,2,2,2,2,2,2,2,2,2,2,2,2,2,2,2,2,2,2,2,2,
2,2,2,2,2,2,2,2,2,2,2,2,2,2,2,2,2,2,2,2,2,2,2,2,2,2,2,2,2,2,2,2,2,2,2,2,
2,4),(-3.40057646114791,-3.3780758375725,-3.36840278722896,-3.36439526785602,
-3.36139066010006,-3.36003268291409,-3.35900778506154,-3.35805801068777,
-3.35676422234127,-3.35355406154749,-3.31732904006563,-3.25931176082143,
-3.20442000492122,-3.19964546742521,-3.19851778925455,-3.19787109583537,
-3.19731006463557,-3.19661289279918,-3.19554052128646,-3.19073688093825,
-3.09832867860021,-3.05734155849525,-3.04620138352563,-3.04174970751654,
-3.0384784757685,-3.03707203272324,-3.03603828474931,-3.03509933095838,
-3.03384862317527,-3.03069334908051,-2.9997172075566,-2.9073834549355,-2.88585953030803,
-2.87691742550064,-2.87556570906745,-2.87487069761884,-2.87436349810518,
-2.87381334287839,-2.87284465653319,-2.87002961105812,-2.82258056836125,
-2.76553546368132,-2.74376287413353,-2.72046257855111,-2.71740968374126,
-2.71500027297125,-2.71376159515059,-2.71284869005617,-2.71187876017533,
-2.71023148262299,-2.70580415276338,-2.63426635093943,-2.59485501008328,
-2.55547466289783,-2.55306270362863,-2.5521834029862,-2.55159179444874,
-2.55101850171338,-2.55032804948362,-2.54860802356007,-2.53299904863972,
-2.53178136180014,-2.52719285099008,-2.51082670325984,-2.43744959529829,
-2.39948166775018,-2.39540070561707,-2.39234956544545,-2.39098399974005,
-2.38995768692751,-2.38900967660309,-2.38772299610491,-2.38520569491823,
-2.36547304665328,-2.35916863505314,-2.31965368483067,-2.29150191595262,
-2.23174377692246,-2.22989088471125,-2.22910016632392,-2.22852629161711,
-2.22799716987455,-2.22727496350389,-2.22584954038574,-2.2142939055225,
-2.12000667675021,-2.09061033387173,-2.07151651223088,-2.06899302358442,
-2.0677247414752,-2.06681130988596,-2.06584317093537,-2.06447990860073,
-2.06165713416645,-2.03140669551207,-1.99870026317578,-1.91238098137092,
-1.90773273885563,-1.90659111469871,-1.90587251143088,-1.9053094776008,
-1.90467691294312,-1.90361277126463,-1.89959162510923,-1.87091329328997,
-1.75279313579684,-1.74703576206788,-1.74520218219657,-1.74419513535759,
-1.74318978669074,-1.74195629503858,-1.73959979183382,-1.72521372622106,
-1.69391427539177,-1.64349039658081,-1.58747708851794,-1.58414250765324,
-1.58310566475482,-1.5825418493938,-1.58199208355738,-1.58138143495541,
-1.58019275912579,-1.57871983899557,-1.52439730404018,-1.50196938745237,
-1.4285183148996,-1.42382087528214,-1.42213282314433,-1.42115497894894,
-1.42024486927613,-1.41900056264828,-1.41659254089449,-1.40093136737134,
-1.3702925990382),.UNSPECIFIED.);
#74=B_SPLINE_CURVE_WITH_KNOTS('',3,(#10786,#10787,#10788,#10789,#10790,
#10791,#10792,#10793,#10794,#10795,#10796,#10797,#10798,#10799,#10800,#10801,
#10802,#10803,#10804,#10805,#10806,#10807,#10808,#10809,#10810,#10811,#10812,
#10813,#10814,#10815,#10816,#10817,#10818,#10819,#10820,#10821,#10822,#10823,
#10824,#10825,#10826,#10827,#10828,#10829,#10830,#10831,#10832,#10833,#10834,
#10835,#10836,#10837,#10838,#10839,#10840,#10841,#10842,#10843,#10844,#10845,
#10846,#10847,#10848,#10849,#10850,#10851,#10852,#10853,#10854,#10855,#10856,
#10857,#10858,#10859,#10860,#10861,#10862,#10863,#10864,#10865,#10866,#10867,
#10868,#10869,#10870,#10871,#10872,#10873,#10874,#10875,#10876,#10877,#10878,
#10879,#10880,#10881,#10882,#10883,#10884,#10885,#10886,#10887,#10888,#10889,
#10890,#10891,#10892,#10893,#10894,#10895,#10896,#10897,#10898,#10899,#10900,
#10901,#10902,#10903,#10904,#10905,#10906,#10907,#10908,#10909,#10910,#10911,
#10912,#10913,#10914,#10915,#10916,#10917,#10918,#10919,#10920,#10921,#10922,
#10923,#10924,#10925,#10926,#10927,#10928,#10929,#10930,#10931,#10932,#10933,
#10934,#10935,#10936,#10937,#10938,#10939,#10940,#10941,#10942,#10943,#10944,
#10945,#10946,#10947,#10948,#10949,#10950,#10951,#10952,#10953,#10954,#10955,
#10956,#10957,#10958,#10959,#10960,#10961,#10962,#10963,#10964,#10965,#10966,
#10967,#10968,#10969,#10970,#10971,#10972,#10973,#10974,#10975,#10976,#10977,
#10978,#10979,#10980,#10981,#10982,#10983,#10984,#10985,#10986,#10987,#10988,
#10989,#10990,#10991,#10992,#10993,#10994,#10995,#10996,#10997,#10998,#10999,
#11000,#11001,#11002,#11003,#11004,#11005,#11006,#11007,#11008,#11009,#11010,
#11011,#11012,#11013,#11014,#11015,#11016,#11017,#11018,#11019,#11020,#11021,
#11022,#11023,#11024,#11025,#11026,#11027,#11028,#11029,#11030,#11031,#11032,
#11033,#11034,#11035,#11036,#11037,#11038,#11039,#11040,#11041,#11042,#11043,
#11044,#11045,#11046,#11047,#11048,#11049,#11050,#11051,#11052,#11053,#11054,
#11055,#11056,#11057,#11058,#11059),.UNSPECIFIED.,.F.,.F.,(4,2,2,2,2,2,
2,2,2,2,2,2,2,2,2,2,2,2,2,2,2,2,2,2,2,2,2,2,2,2,2,2,2,2,2,2,2,2,2,2,2,2,
2,2,2,2,2,2,2,2,2,2,2,2,2,2,2,2,2,2,2,2,2,2,2,2,2,2,2,2,2,2,2,2,2,2,2,2,
2,2,2,2,2,2,2,2,2,2,2,2,2,2,2,2,2,2,2,2,2,2,2,2,2,2,2,2,2,2,2,2,2,2,2,2,
2,2,2,2,2,2,2,2,2,2,2,2,2,2,2,2,2,2,2,2,2,2,4),(-2.69255696121762,-2.67347825365679,
-2.58627168165284,-2.56149935779709,-2.54871425959265,-2.54641935350897,
-2.54519901389999,-2.54419449474869,-2.54317989025542,-2.54130844106319,
-2.53524468708342,-2.53382390960164,-2.53032962086112,-2.52891162285775,
-2.52695364768927,-2.52638753891779,-2.52430067698228,-2.52283416157334,
-2.52162851903848,-2.43863644977151,-2.38689160927336,-2.38459379329566,
-2.38373349105708,-2.38314223414127,-2.38256896794985,-2.38187818563985,
-2.38015544412112,-2.36443917379122,-2.36316922629901,-2.36036926766921,
-2.33089201040431,-2.30943930201984,-2.26127805319402,-2.23771083080318,
-2.22575006705512,-2.2235092113134,-2.22230036069438,-2.22130564404892,
-2.22028621102971,-2.21839117853824,-2.21213174163553,-2.10603927950583,
-2.06406759692736,-2.06161860087352,-2.06073403343725,-2.06014132686672,
-2.05956890896528,-2.05888173030109,-2.05724612486324,-2.04365574694947,
-2.04264276182633,-2.04175486668268,-2.03980651095245,-2.03163715773507,
-2.00666100196485,-1.9321063232717,-1.90397608063725,-1.90089649835486,
-1.89965811561594,-1.89862846601625,-1.89757540094881,-1.89604310966808,
-1.89202774447157,-1.83842965554268,-1.74401127242429,-1.73915707855529,
-1.7380804923654,-1.73738194892242,-1.73682073384261,-1.73617485361328,
-1.7350511371394,-1.73032903796948,-1.68862554964978,-1.58501101641814,
-1.57878582148155,-1.5768946391431,-1.57587586821121,-1.57489139084082,
-1.57378044474401,-1.57172400210714,-1.56920970632291,-1.50931814281801,
-1.42059534518491,-1.41590881346204,-1.41484591730983,-1.41415164371323,
-1.41364679943432,-1.41301741940066,-1.41196762672463,-1.40809999507898,
-1.31951541095213,-1.25872899378092,-1.25491189372383,-1.25351877264869,
-1.25254242039694,-1.2515506176788,-1.25028713834807,-1.24890899174348,
-1.24667458029896,-1.24227469835377,-1.19900755503168,-1.11838292016377,
-1.1147739056282,-1.10971912165377,-1.0936723088765,-1.09196223365962,-1.09126180524186,
-1.09073813577941,-1.0901592269365,-1.08934194338152,-1.08733263624776,
-1.07582970671104,-1.05011163146483,-0.94025281949781,-0.938009259376781,
-0.932295131056112,-0.930466905752835,-0.929460849025636,-0.928459893107989,
-0.927251225905809,-0.924981745348664,-0.922144062674089,-0.916062186601247,
-0.899111483269984,-0.850763426831215,-0.774075947140235,-0.77303897685378,
-0.76941738138719,-0.768346310796388,-0.767775522739613,-0.767220581802722,
-0.766539180666425,-0.765252084217158,-0.757842297137281,-0.742329307309087,
-0.692272519594694,-0.661978904396988),.UNSPECIFIED.);
#75=B_SPLINE_CURVE_WITH_KNOTS('',3,(#11065,#11066,#11067,#11068,#11069,
#11070,#11071,#11072,#11073,#11074,#11075,#11076,#11077,#11078,#11079,#11080,
#11081,#11082,#11083,#11084,#11085,#11086,#11087,#11088,#11089,#11090,#11091,
#11092,#11093,#11094,#11095,#11096,#11097,#11098,#11099,#11100,#11101,#11102,
#11103,#11104,#11105,#11106,#11107,#11108,#11109,#11110,#11111,#11112,#11113,
#11114,#11115,#11116,#11117,#11118,#11119,#11120,#11121,#11122,#11123,#11124,
#11125,#11126,#11127,#11128,#11129,#11130,#11131,#11132,#11133,#11134,#11135,
#11136,#11137,#11138,#11139,#11140,#11141,#11142,#11143,#11144,#11145,#11146,
#11147,#11148,#11149,#11150,#11151,#11152,#11153,#11154,#11155,#11156,#11157,
#11158,#11159,#11160,#11161,#11162,#11163,#11164,#11165,#11166,#11167,#11168,
#11169,#11170,#11171,#11172,#11173,#11174,#11175,#11176,#11177,#11178,#11179,
#11180,#11181,#11182,#11183,#11184,#11185,#11186,#11187,#11188,#11189,#11190,
#11191,#11192,#11193,#11194,#11195,#11196,#11197,#11198,#11199,#11200,#11201,
#11202,#11203,#11204,#11205,#11206,#11207,#11208,#11209,#11210,#11211,#11212,
#11213,#11214,#11215,#11216,#11217,#11218,#11219,#11220,#11221,#11222,#11223,
#11224,#11225,#11226,#11227,#11228,#11229,#11230,#11231,#11232,#11233,#11234,
#11235,#11236,#11237,#11238,#11239,#11240,#11241,#11242,#11243,#11244,#11245,
#11246,#11247,#11248,#11249,#11250,#11251,#11252,#11253,#11254,#11255,#11256,
#11257,#11258,#11259,#11260,#11261,#11262,#11263,#11264,#11265,#11266,#11267,
#11268,#11269,#11270,#11271,#11272,#11273,#11274,#11275,#11276,#11277,#11278),
 .UNSPECIFIED.,.F.,.F.,(4,2,2,2,2,2,2,2,2,2,2,2,2,2,2,2,2,2,2,2,2,2,2,2,
2,2,2,2,2,2,2,2,2,2,2,2,2,2,2,2,2,2,2,2,2,2,2,2,2,2,2,2,2,2,2,2,2,2,2,2,
2,2,2,2,2,2,2,2,2,2,2,2,2,2,2,2,2,2,2,2,2,2,2,2,2,2,2,2,2,2,2,2,2,2,2,2,
2,2,2,2,2,2,2,2,2,2,4),(-1.36955217660447,-1.35438198264554,-1.25171466928822,
-1.25033018241312,-1.24914578420268,-1.24301205659692,-1.23878392598788,
-1.23716839589181,-1.23620494527356,-1.23529005058641,-1.23403597046894,
-1.23155997848618,-1.22839810301241,-1.20364425443094,-1.16867765533724,
-1.08136737778924,-1.07656897407976,-1.07549716123163,-1.07480024117134,
-1.07423933653693,-1.07359270291284,-1.07246491629994,-1.06768689371836,
-1.01284384328921,-0.942114783682391,-0.938532701363764,-0.917968568710297,
-0.915138967765725,-0.913824413434402,-0.912807518047145,-0.911866303834704,
-0.910303617717483,-0.906056780776339,-0.899891974116983,-0.882628837322805,
-0.832110521666651,-0.757878793394048,-0.753557253638437,-0.752425300070153,
-0.751770959267558,-0.751210624089526,-0.750523531878927,-0.749209144944406,
-0.741190293935152,-0.738233644375573,-0.708836955097061,-0.637043657867222,
-0.619994283552344,-0.614485917866933,-0.61316077870147,-0.611957685387143,
-0.610340246165035,-0.608271667092593,-0.607313404898065,-0.606954649605142,
-0.604895585846466,-0.603068038590231,-0.595302423768686,-0.592609148376004,
-0.591278027862611,-0.590318600232067,-0.5892998263656,-0.588302580971732,
-0.58601675705447,-0.573027783792601,-0.548746586826365,-0.517863639930038,
-0.441029531642349,-0.438542062858685,-0.431056438844321,-0.429807528471815,
-0.429064682762545,-0.428496772427648,-0.427883186691457,-0.426903424071744,
-0.423705627302623,-0.375612653486214,-0.349181283099561,-0.317951095689469,
-0.299029579476036,-0.292124685105148,-0.290630298769369,-0.289435352112233,
-0.285481070328898,-0.284903076009555,-0.283105697494471,-0.281984092017214,
-0.279456172279823,-0.271022965258246,-0.269113986430642,-0.267866539798169,
-0.266860117346127,-0.265913977110473,-0.264790170791789,-0.261315824987277,
-0.227785563293494,-0.207412476083892,-0.112675597240101,-0.107768758366129,
-0.10668800903978,-0.105988198957318,-0.105426928374396,-0.104782055466478,
-0.103662735871478,-0.098995661539217,-0.077082042319963,-0.000962379967314271),
 .UNSPECIFIED.);
#76=B_SPLINE_CURVE_WITH_KNOTS('',3,(#11279,#11280,#11281,#11282,#11283,
#11284,#11285,#11286,#11287,#11288,#11289,#11290,#11291,#11292,#11293,#11294,
#11295,#11296,#11297,#11298,#11299,#11300,#11301,#11302,#11303,#11304,#11305,
#11306,#11307,#11308,#11309,#11310,#11311,#11312,#11313,#11314,#11315,#11316,
#11317,#11318,#11319,#11320,#11321,#11322,#11323,#11324,#11325,#11326,#11327,
#11328,#11329,#11330,#11331,#11332,#11333,#11334,#11335,#11336,#11337,#11338,
#11339,#11340,#11341,#11342,#11343,#11344,#11345,#11346,#11347,#11348,#11349,
#11350,#11351,#11352,#11353,#11354,#11355,#11356,#11357,#11358,#11359,#11360,
#11361,#11362,#11363,#11364,#11365,#11366,#11367,#11368,#11369,#11370),
 .UNSPECIFIED.,.F.,.F.,(4,2,2,2,2,2,2,2,2,2,2,2,2,2,2,2,2,2,2,2,2,2,2,2,
2,2,2,2,2,2,2,2,2,2,2,2,2,2,2,2,2,2,2,2,2,4),(-4.06187856554517,-4.01028312517064,
-4.00820489509965,-4.0068923922961,-4.0058928370161,-4.00487275991072,-4.00391515288097,
-4.00259138783777,-3.99920542054684,-3.9525570417565,-3.94657911598626,
-3.88751088390632,-3.84654652891285,-3.84480147835424,-3.84402993595295,
-3.84345941770221,-3.84292550177109,-3.84218492111564,-3.84068664078943,
-3.82688268891551,-3.74615381186573,-3.7159189363492,-3.69966566393637,
-3.68621704629759,-3.68390936706516,-3.68290969500177,-3.68188956907854,
-3.6809321172671,-3.6796088846704,-3.67622598294025,-3.62977230807033,-3.58097983958198,
-3.57477522245894,-3.56738464730999,-3.54128548606904,-3.52895553115468,
-3.5227682477937,-3.5215455595657,-3.52087802652391,-3.5203734036592,-3.51972328912141,
-3.5186097497611,-3.51447447247373,-3.44129701154587,-3.41074387972596,
-3.40057646114791),.UNSPECIFIED.);
#77=B_SPLINE_CURVE_WITH_KNOTS('',3,(#11372,#11373,#11374,#11375,#11376,
#11377,#11378,#11379,#11380,#11381,#11382,#11383,#11384,#11385,#11386,#11387,
#11388,#11389,#11390,#11391,#11392,#11393,#11394,#11395,#11396,#11397,#11398,
#11399,#11400,#11401,#11402,#11403,#11404,#11405,#11406,#11407,#11408,#11409,
#11410,#11411,#11412,#11413,#11414,#11415,#11416,#11417,#11418,#11419,#11420,
#11421,#11422,#11423,#11424,#11425,#11426,#11427,#11428,#11429,#11430,#11431,
#11432,#11433,#11434,#11435,#11436,#11437,#11438,#11439,#11440,#11441,#11442,
#11443,#11444,#11445,#11446,#11447,#11448,#11449,#11450,#11451,#11452,#11453,
#11454,#11455,#11456,#11457,#11458,#11459,#11460,#11461,#11462,#11463,#11464,
#11465,#11466,#11467,#11468,#11469,#11470,#11471,#11472,#11473,#11474,#11475,
#11476,#11477,#11478,#11479,#11480,#11481,#11482,#11483,#11484,#11485),
 .UNSPECIFIED.,.F.,.F.,(4,2,2,2,2,2,2,2,2,2,2,2,2,2,2,2,2,2,2,2,2,2,2,2,
2,2,2,2,2,2,2,2,2,2,2,2,2,2,2,2,2,2,2,2,2,2,2,2,2,2,2,2,2,2,2,2,4),(-0.661978904396988,
-0.627113612311915,-0.625151163231897,-0.62348303709909,-0.62290918167699,
-0.620856007709331,-0.618943009507162,-0.610528516700987,-0.608266312585233,
-0.606925688624173,-0.605904347407471,-0.604962839063766,-0.6034324881459,
-0.599407480486424,-0.593643195553803,-0.577872309154318,-0.542083767646264,
-0.451494885974086,-0.44661902210718,-0.44554068247425,-0.444841586676769,
-0.444280321015988,-0.443634820720731,-0.44251284879718,-0.437813133082642,
-0.396765190853775,-0.361946912313917,-0.34265857858922,-0.312600887769801,
-0.307916047922302,-0.306381113769936,-0.305185331643166,-0.301966963503426,
-0.300776472795027,-0.298770439246987,-0.2972617768537,-0.293642477561785,
-0.286617164155146,-0.284658728239131,-0.283500186979867,-0.282497224578451,
-0.281533106752897,-0.27958565297195,-0.271909090059396,-0.258705282415628,
-0.235142472812011,-0.185650843905423,-0.135759820580576,-0.124318912392373,
-0.12274003009909,-0.122007385789521,-0.121440896279995,-0.120822250592115,
-0.119820473506015,-0.116426053729279,-0.094944610367713,-0.000962465205791075),
 .UNSPECIFIED.);
#78=B_SPLINE_CURVE_WITH_KNOTS('',3,(#11486,#11487,#11488,#11489,#11490,
#11491,#11492,#11493,#11494,#11495,#11496,#11497,#11498,#11499,#11500,#11501,
#11502,#11503,#11504,#11505,#11506,#11507,#11508,#11509,#11510,#11511,#11512,
#11513,#11514,#11515,#11516,#11517,#11518,#11519,#11520,#11521,#11522,#11523,
#11524,#11525,#11526,#11527,#11528,#11529,#11530,#11531,#11532,#11533,#11534,
#11535,#11536,#11537,#11538,#11539,#11540,#11541,#11542,#11543,#11544,#11545,
#11546,#11547,#11548,#11549,#11550,#11551,#11552,#11553,#11554,#11555,#11556,
#11557,#11558,#11559,#11560,#11561,#11562,#11563,#11564,#11565,#11566,#11567,
#11568,#11569,#11570,#11571,#11572,#11573,#11574,#11575,#11576,#11577,#11578,
#11579,#11580,#11581,#11582,#11583,#11584,#11585,#11586,#11587,#11588,#11589,
#11590,#11591,#11592,#11593,#11594,#11595,#11596,#11597,#11598,#11599,#11600,
#11601,#11602,#11603,#11604,#11605,#11606,#11607,#11608,#11609,#11610,#11611,
#11612,#11613,#11614,#11615,#11616,#11617,#11618,#11619,#11620,#11621,#11622,
#11623,#11624,#11625,#11626,#11627,#11628,#11629,#11630,#11631,#11632,#11633,
#11634,#11635,#11636,#11637,#11638,#11639,#11640,#11641,#11642,#11643,#11644,
#11645,#11646,#11647,#11648,#11649,#11650,#11651,#11652,#11653,#11654,#11655,
#11656,#11657,#11658,#11659,#11660,#11661,#11662,#11663,#11664,#11665,#11666,
#11667,#11668,#11669,#11670,#11671,#11672,#11673,#11674,#11675,#11676,#11677,
#11678,#11679,#11680,#11681,#11682,#11683,#11684,#11685,#11686,#11687,#11688,
#11689,#11690,#11691,#11692,#11693),.UNSPECIFIED.,.F.,.F.,(4,2,2,2,2,2,
2,2,2,2,2,2,2,2,2,2,2,2,2,2,2,2,2,2,2,2,2,2,2,2,2,2,2,2,2,2,2,2,2,2,2,2,
2,2,2,2,2,2,2,2,2,2,2,2,2,2,2,2,2,2,2,2,2,2,2,2,2,2,2,2,2,2,2,2,2,2,2,2,
2,2,2,2,2,2,2,2,2,2,2,2,2,2,2,2,2,2,2,2,2,2,2,2,2,4),(-4.06320052515722,
-4.02854659369987,-4.02599157095642,-4.02447993867694,-4.02340400408273,
-4.02246226240333,-4.02144475844287,-4.02012926886495,-4.01729707730144,
-3.99669577433376,-3.99312836322317,-3.98530089655057,-3.97963874261392,
-3.88624641242043,-3.8704720939628,-3.86288476576896,-3.86158897077024,
-3.8609055477264,-3.86035029452704,-3.85969415400662,-3.85855553514836,
-3.8541705904117,-3.85152464773105,-3.84994677000181,-3.84859115908881,
-3.75448400553711,-3.73323402184924,-3.71332681142404,-3.70286602615713,
-3.70071681448195,-3.69973324466078,-3.69876000633362,-3.69779226512787,
-3.69643140569658,-3.6936195848049,-3.66387448893644,-3.61235814755693,
-3.60669416211047,-3.60022607679449,-3.59270528889197,-3.54058024380383,
-3.53874399284793,-3.53795603208496,-3.53738251282187,-3.53685251236143,
-3.53612733400141,-3.53469069499509,-3.52282235557942,-3.4500196497108,
-3.41731444533606,-3.39305972575065,-3.38451997204443,-3.38086718866179,
-3.37891645798891,-3.37724671847994,-3.37617286166545,-3.37515480795055,
-3.37383603810287,-3.37098673137131,-3.34995425528351,-3.34772134843608,
-3.26007371048579,-3.24805499743998,-3.22583736628036,-3.21672609650072,
-3.21536768741551,-3.21467111370844,-3.21410988571839,-3.21346220395574,
-3.2123599241163,-3.20833776362933,-3.14026803353591,-3.09383598516356,
-3.06930428855282,-3.06114459270299,-3.05761346013487,-3.05490057619976,
-3.05359939075846,-3.05263339336126,-3.05167625924942,-3.05035532632213,
-3.04698823597713,-3.00171040552554,-2.95208950291395,-2.89643105074264,
-2.89301061865856,-2.89200587526018,-2.89138646188723,-2.89082000728871,
-2.89008841060147,-2.88851563696069,-2.87723505703119,-2.87498944770347,
-2.87402207025079,-2.79055858921925,-2.73577857512061,-2.73331283961937,
-2.7318380947509,-2.7305058327933,-2.72950310380974,-2.72854969004676,-2.72724288730549,
-2.72395893684818,-2.69352985927485),.UNSPECIFIED.);
#79=B_SPLINE_CURVE_WITH_KNOTS('',3,(#11698,#11699,#11700,#11701,#11702,
#11703,#11704,#11705,#11706,#11707,#11708,#11709,#11710,#11711,#11712,#11713,
#11714,#11715,#11716,#11717,#11718,#11719,#11720,#11721,#11722,#11723,#11724,
#11725,#11726,#11727,#11728,#11729,#11730,#11731,#11732,#11733,#11734,#11735,
#11736,#11737,#11738,#11739,#11740,#11741,#11742,#11743,#11744,#11745,#11746,
#11747,#11748,#11749,#11750,#11751,#11752,#11753,#11754,#11755,#11756,#11757,
#11758,#11759,#11760,#11761,#11762,#11763,#11764,#11765,#11766,#11767,#11768,
#11769,#11770,#11771,#11772,#11773,#11774,#11775,#11776,#11777,#11778,#11779,
#11780,#11781,#11782,#11783,#11784,#11785,#11786,#11787,#11788,#11789,#11790,
#11791,#11792,#11793,#11794,#11795,#11796,#11797,#11798,#11799,#11800,#11801,
#11802,#11803,#11804,#11805,#11806,#11807,#11808,#11809,#11810,#11811,#11812,
#11813,#11814,#11815,#11816,#11817,#11818,#11819,#11820,#11821,#11822,#11823,
#11824,#11825,#11826,#11827,#11828,#11829,#11830,#11831,#11832,#11833,#11834,
#11835,#11836,#11837,#11838,#11839,#11840,#11841,#11842,#11843,#11844,#11845,
#11846,#11847,#11848,#11849,#11850,#11851,#11852,#11853,#11854,#11855,#11856,
#11857,#11858,#11859,#11860,#11861,#11862,#11863,#11864,#11865,#11866,#11867,
#11868,#11869,#11870,#11871,#11872,#11873,#11874,#11875,#11876,#11877,#11878,
#11879,#11880,#11881,#11882,#11883,#11884,#11885,#11886,#11887,#11888,#11889,
#11890,#11891,#11892,#11893,#11894,#11895,#11896,#11897,#11898,#11899,#11900,
#11901,#11902,#11903,#11904,#11905,#11906,#11907,#11908,#11909,#11910,#11911,
#11912,#11913,#11914,#11915,#11916,#11917,#11918,#11919,#11920,#11921,#11922,
#11923,#11924,#11925,#11926,#11927,#11928,#11929,#11930,#11931,#11932,#11933,
#11934,#11935,#11936,#11937,#11938,#11939,#11940,#11941,#11942,#11943,#11944,
#11945,#11946,#11947,#11948,#11949,#11950,#11951,#11952,#11953,#11954,#11955,
#11956,#11957,#11958,#11959,#11960,#11961,#11962,#11963,#11964,#11965,#11966,
#11967,#11968,#11969,#11970,#11971,#11972,#11973,#11974,#11975,#11976,#11977,
#11978,#11979,#11980,#11981,#11982,#11983,#11984,#11985,#11986,#11987,#11988,
#11989,#11990,#11991,#11992,#11993,#11994,#11995,#11996,#11997,#11998,#11999),
 .UNSPECIFIED.,.F.,.F.,(4,2,2,2,2,2,2,2,2,2,2,2,2,2,2,2,2,2,2,2,2,2,2,2,
2,2,2,2,2,2,2,2,2,2,2,2,2,2,2,2,2,2,2,2,2,2,2,2,2,2,2,2,2,2,2,2,2,2,2,2,
2,2,2,2,2,2,2,2,2,2,2,2,2,2,2,2,2,2,2,2,2,2,2,2,2,2,2,2,2,2,2,2,2,2,2,2,
2,2,2,2,2,2,2,2,2,2,2,2,2,2,2,2,2,2,2,2,2,2,2,2,2,2,2,2,2,2,2,2,2,2,2,2,
2,2,2,2,2,2,2,2,2,2,2,2,2,2,2,2,2,2,4),(-3.39969022993959,-3.3786984878877,
-3.35948849290766,-3.34588685838186,-3.34066440146017,-3.33741257346593,
-3.33667800306114,-3.33599027095376,-3.33542991438605,-3.33486178715339,
-3.33380349977984,-3.33029044840005,-3.27407115351213,-3.23037848365561,
-3.19417663529458,-3.1785634569545,-3.17617159355712,-3.17491717091749,
-3.17400575597167,-3.17303227208262,-3.1716490720901,-3.16789482769006,
-3.1111685143221,-3.04883083834845,-3.01879730840282,-3.01469228204835,
-3.01361069668949,-3.01297432080491,-3.01241208527157,-3.01170007109684,
-3.01057962584175,-3.00803289862645,-2.95743123880408,-2.89036843290398,
-2.88079374861989,-2.85644449364307,-2.85354392084936,-2.85218550142441,
-2.85116523679675,-2.85020843480577,-2.84888733181381,-2.84551645678593,
-2.79985844443754,-2.72383796005469,-2.70139477583681,-2.69224033718215,
-2.69088518689225,-2.69018377698549,-2.68967584873648,-2.68912875353269,
-2.68833957542714,-2.68612486896696,-2.65176470822932,-2.57959614065157,
-2.55146179005225,-2.53912698298267,-2.53183584758135,-2.5299242234798,
-2.5287790683472,-2.52777253658323,-2.52652335916783,-2.52460876611352,
-2.51610554048112,-2.42034506873497,-2.39568997735949,-2.37218284936963,
-2.36981326432523,-2.36809663853903,-2.36730595152729,-2.36673211313041,
-2.36620303475001,-2.36548090202363,-2.36405566770089,-2.35250576326666,
-2.34899396760495,-2.25827081396586,-2.22885301940535,-2.20975161615233,
-2.20722801904973,-2.20595975867361,-2.20504637292322,-2.20407831055815,
-2.2027152019381,-2.19989289495155,-2.19231065962865,-2.19049665751667,
-2.18843335879618,-2.1879774800841,-2.18595995267805,-2.1842444171534,-2.18005147146979,
-2.17600593781256,-2.13071837941265,-2.0491810894737,-2.04555416463119,
-2.04452818154351,-2.04390419560876,-2.04333935203872,-2.042617587916,-2.04109496590049,
-2.0309832034178,-2.0038184010449,-1.91302938216084,-1.90676618036601,-1.90509849742528,
-1.90388230575305,-1.90277294404895,-1.88685573810697,-1.88423103243504,
-1.88294229078672,-1.88193175961283,-1.8808110993466,-1.87897010541056,
-1.87246659847572,-1.83119558278224,-1.7468639512005,-1.74290785871373,
-1.74173322294893,-1.73871648379443,-1.72360881608827,-1.72207368100775,
-1.72132394702616,-1.72078759294804,-1.72027546718284,-1.71954576601438,
-1.71802253485886,-1.70231312007715,-1.68480950659857,-1.56814511771077,
-1.56227450805133,-1.56042673025002,-1.55941684969971,-1.55841184490607,
-1.55720811082083,-1.55496048900531,-1.55215631988702,-1.53205293842959,
-1.4953197925989,-1.42967105561337,-1.41926180505218,-1.41767793565167,
-1.4168456357559,-1.40051394412944,-1.39894702510061,-1.39818954967374,
-1.3976511820023,-1.39714015844877,-1.3964168464538,-1.39492552270816,-1.3809138042181,
-1.36955217660447),.UNSPECIFIED.);
#80=B_SPLINE_CURVE_WITH_KNOTS('',3,(#12000,#12001,#12002,#12003,#12004,
#12005,#12006,#12007,#12008,#12009,#12010,#12011,#12012,#12013,#12014,#12015,
#12016,#12017,#12018,#12019,#12020,#12021,#12022,#12023,#12024,#12025,#12026,
#12027,#12028,#12029,#12030,#12031,#12032,#12033,#12034,#12035,#12036,#12037,
#12038,#12039,#12040,#12041,#12042,#12043,#12044,#12045,#12046,#12047,#12048,
#12049,#12050,#12051,#12052,#12053,#12054,#12055,#12056,#12057,#12058,#12059,
#12060,#12061,#12062,#12063,#12064,#12065,#12066,#12067,#12068,#12069,#12070,
#12071,#12072,#12073,#12074,#12075,#12076,#12077,#12078,#12079,#12080,#12081,
#12082,#12083,#12084,#12085,#12086,#12087,#12088,#12089,#12090,#12091,#12092,
#12093,#12094,#12095,#12096,#12097,#12098,#12099,#12100,#12101,#12102,#12103,
#12104,#12105,#12106,#12107,#12108,#12109,#12110,#12111,#12112,#12113,#12114,
#12115,#12116,#12117,#12118,#12119,#12120,#12121,#12122,#12123,#12124,#12125,
#12126,#12127,#12128,#12129,#12130,#12131,#12132,#12133,#12134,#12135,#12136,
#12137,#12138,#12139,#12140,#12141,#12142,#12143,#12144,#12145,#12146,#12147,
#12148,#12149,#12150,#12151,#12152,#12153,#12154,#12155,#12156,#12157,#12158,
#12159,#12160,#12161,#12162,#12163,#12164,#12165,#12166,#12167,#12168,#12169,
#12170,#12171,#12172,#12173,#12174,#12175,#12176,#12177,#12178,#12179,#12180,
#12181,#12182,#12183,#12184,#12185,#12186,#12187,#12188,#12189,#12190,#12191,
#12192,#12193,#12194,#12195,#12196,#12197,#12198,#12199,#12200,#12201,#12202,
#12203,#12204,#12205,#12206,#12207,#12208,#12209,#12210,#12211,#12212,#12213,
#12214,#12215,#12216,#12217,#12218,#12219,#12220,#12221,#12222,#12223,#12224,
#12225,#12226,#12227,#12228,#12229,#12230,#12231,#12232,#12233,#12234,#12235,
#12236,#12237,#12238,#12239,#12240,#12241,#12242,#12243,#12244,#12245,#12246,
#12247,#12248,#12249,#12250,#12251,#12252,#12253,#12254,#12255,#12256,#12257),
 .UNSPECIFIED.,.F.,.F.,(4,2,2,2,2,2,2,2,2,2,2,2,2,2,2,2,2,2,2,2,2,2,2,2,
2,2,2,2,2,2,2,2,2,2,2,2,2,2,2,2,2,2,2,2,2,2,2,2,2,2,2,2,2,2,2,2,2,2,2,2,
2,2,2,2,2,2,2,2,2,2,2,2,2,2,2,2,2,2,2,2,2,2,2,2,2,2,2,2,2,2,2,2,2,2,2,2,
2,2,2,2,2,2,2,2,2,2,2,2,2,2,2,2,2,2,2,2,2,2,2,2,2,2,2,2,2,2,2,2,4),(-2.69352985927485,
-2.68389408092132,-2.60895562576247,-2.57442617333315,-2.57001717621488,
-2.56891863774995,-2.56827823318252,-2.56771617440436,-2.56700928507732,
-2.56590617795353,-2.56117999440359,-2.46394710576004,-2.41681557895182,
-2.41220764718302,-2.40989587106581,-2.40848521826122,-2.40719934367583,
-2.40620397129558,-2.40523627289003,-2.4038755451556,-2.40106422809616,
-2.37133936304647,-2.3603291951398,-2.3343502247734,-2.31454743131305,-2.27191343437527,
-2.25012374099055,-2.246699990916,-2.24569497922519,-2.24507555973505,-2.24450920989543,
-2.24377789824917,-2.24256862938517,-2.23804864061365,-2.14719133378575,
-2.08851797323181,-2.08553160793023,-2.08417263674111,-2.0831519485819,
-2.0821947427239,-2.08087307150257,-2.07750068975277,-2.03181498087369,
-1.98056479987243,-1.92702006997968,-1.92363794576221,-1.92259502376976,
-1.92202982800443,-1.92152501194605,-1.92085668661933,-1.91963091765707,
-1.91339528336818,-1.90093649743885,-1.87739211464657,-1.76965303694037,
-1.76349706667714,-1.7616140385948,-1.76059684980213,-1.7595920855993,-1.75837477271154,
-1.75609539301282,-1.74339496883304,-1.71859441017217,-1.62915304762118,
-1.60187371291614,-1.59994212688075,-1.59919663265854,-1.59866134308105,
-1.59810283215021,-1.59735829862927,-1.59653133042307,-1.59514148102259,
-1.56367441790498,-1.44590148758449,-1.44010022486342,-1.43826091523625,
-1.43725261591757,-1.43624723253123,-1.43501548018086,-1.43266774869513,
-1.41849163181968,-1.3882140135813,-1.33839842020177,-1.28083526847851,
-1.27723866545663,-1.27617050602013,-1.27560032105911,-1.27505170089691,
-1.27438590571161,-1.2736687765961,-1.2725425666678,-1.27039683871987,-1.25054747273822,
-1.23743471056791,-1.16003570544902,-1.14806361545362,-1.11924620331764,
-1.11618834952474,-1.11493276805087,-1.11399259596314,-1.11295992814161,
-1.11153072021232,-1.10815124861225,-1.10355545695711,-1.05663818122653,
-0.965110746092647,-0.954966681861803,-0.953442507424782,-0.952720396319068,
-0.952168323258122,-0.951560783861697,-0.950586321666152,-0.949432248676162,
-0.947213137913438,-0.941815696279655,-0.925302507687756,-0.901010654267849,
-0.835269718565094,-0.819460834165034,-0.81687248291935,-0.795845331885353,
-0.792996734735651,-0.79167830333446,-0.790660514890877,-0.789564917209215,
-0.787836700103267,-0.782363986452277,-0.690580316824922,-0.662566381801328),
 .UNSPECIFIED.);
#81=B_SPLINE_CURVE_WITH_KNOTS('',3,(#12263,#12264,#12265,#12266,#12267,
#12268,#12269,#12270,#12271,#12272,#12273,#12274,#12275,#12276,#12277,#12278,
#12279,#12280,#12281,#12282,#12283,#12284,#12285,#12286,#12287,#12288,#12289,
#12290,#12291,#12292,#12293,#12294,#12295,#12296,#12297,#12298,#12299,#12300,
#12301,#12302,#12303,#12304,#12305,#12306,#12307,#12308,#12309,#12310,#12311,
#12312,#12313,#12314,#12315,#12316,#12317,#12318,#12319,#12320,#12321,#12322,
#12323,#12324,#12325,#12326,#12327,#12328,#12329,#12330,#12331,#12332,#12333,
#12334,#12335,#12336,#12337,#12338,#12339,#12340,#12341,#12342,#12343,#12344,
#12345,#12346,#12347,#12348,#12349,#12350,#12351,#12352,#12353,#12354,#12355,
#12356,#12357,#12358,#12359,#12360,#12361,#12362,#12363,#12364,#12365,#12366,
#12367,#12368,#12369,#12370,#12371,#12372,#12373,#12374,#12375,#12376,#12377,
#12378,#12379,#12380,#12381,#12382,#12383,#12384,#12385,#12386,#12387,#12388,
#12389,#12390,#12391,#12392,#12393,#12394,#12395,#12396,#12397,#12398,#12399,
#12400,#12401,#12402,#12403,#12404,#12405,#12406,#12407,#12408,#12409,#12410,
#12411,#12412,#12413,#12414,#12415,#12416,#12417,#12418,#12419,#12420,#12421,
#12422,#12423,#12424,#12425,#12426,#12427,#12428,#12429,#12430,#12431,#12432,
#12433,#12434,#12435,#12436,#12437,#12438,#12439,#12440,#12441,#12442,#12443,
#12444,#12445,#12446,#12447,#12448,#12449,#12450,#12451,#12452,#12453,#12454,
#12455,#12456,#12457,#12458,#12459,#12460,#12461,#12462,#12463,#12464,#12465,
#12466,#12467,#12468,#12469,#12470,#12471,#12472),.UNSPECIFIED.,.F.,.F.,
(4,2,2,2,2,2,2,2,2,2,2,2,2,2,2,2,2,2,2,2,2,2,2,2,2,2,2,2,2,2,2,2,2,2,2,
2,2,2,2,2,2,2,2,2,2,2,2,2,2,2,2,2,2,2,2,2,2,2,2,2,2,2,2,2,2,2,2,2,2,2,2,
2,2,2,2,2,2,2,2,2,2,2,2,2,2,2,2,2,2,2,2,2,2,2,2,2,2,2,2,2,2,2,2,2,4),(-1.3700182626362,
-1.36592562693376,-1.32703128660657,-1.25909429378232,-1.21787961320516,
-1.21546755798024,-1.21464948497662,-1.21409426026938,-1.21358817863959,
-1.2129032860087,-1.21162585450702,-1.20478274722828,-1.19054162214828,
-1.16723812606352,-1.10697677551043,-1.08480759494741,-1.07677163629666,
-1.07532377515967,-1.07410481494186,-1.07233361323219,-1.07025749908928,
-1.06713614545577,-1.06401195172129,-1.05616817902585,-1.05412729849195,
-1.05294968001654,-1.05204570821936,-1.05087779711243,-1.04886631659573,
-1.04039844011434,-1.01159811942756,-0.949868610417787,-0.90669708736391,
-0.906325899185845,-0.905417407009432,-0.893732973258678,-0.892165068910575,
-0.891423391432866,-0.890855583658289,-0.890241302265071,-0.889258754608297,
-0.88611724013485,-0.843727933985025,-0.79642093626542,-0.735959297627083,
-0.732167039801404,-0.730777755800238,-0.729802464698541,-0.72889132704975,
-0.727640345236682,-0.725249884435287,-0.709843293116012,-0.69029644310253,
-0.636374030976765,-0.592576630663127,-0.585624928757988,-0.584158212509357,
-0.582852244954422,-0.570808925093855,-0.56920707694905,-0.568470162594901,
-0.567903102066476,-0.567286649447224,-0.566294379877547,-0.563058952118846,
-0.533504230194774,-0.484529409184136,-0.413772855735669,-0.409410560106277,
-0.407773411133712,-0.406805491487863,-0.405891890800374,-0.40462277712555,
-0.403260255069271,-0.396705220210389,-0.385968489064426,-0.347295834274742,
-0.318840352571299,-0.277563615076129,-0.269436645821019,-0.265370862260202,
-0.264340778134366,-0.262008173980406,-0.259906803819862,-0.24787069071717,
-0.246269174766381,-0.24553234569493,-0.244965321982282,-0.244348879722596,
-0.243356564352854,-0.24219154956837,-0.228381061006591,-0.193047608999555,
-0.179385784785977,-0.165160845705691,-0.0914217283366651,-0.0897382975120328,
-0.0861859627833301,-0.0848347804093064,-0.0838698861247194,-0.0829551577119613,
-0.0816781069745883,-0.0803045910796622,-0.0780811396084523,-0.000961462500411059),
 .UNSPECIFIED.);
#82=B_SPLINE_CURVE_WITH_KNOTS('',3,(#12473,#12474,#12475,#12476,#12477,
#12478,#12479,#12480,#12481,#12482,#12483,#12484,#12485,#12486,#12487,#12488,
#12489,#12490,#12491,#12492,#12493,#12494,#12495,#12496,#12497,#12498,#12499,
#12500,#12501,#12502,#12503,#12504,#12505,#12506,#12507,#12508,#12509,#12510,
#12511,#12512,#12513,#12514,#12515,#12516,#12517,#12518,#12519,#12520,#12521,
#12522,#12523,#12524,#12525,#12526,#12527,#12528,#12529,#12530,#12531,#12532,
#12533,#12534,#12535,#12536,#12537,#12538,#12539,#12540,#12541,#12542,#12543,
#12544,#12545,#12546,#12547,#12548,#12549,#12550,#12551,#12552,#12553,#12554,
#12555,#12556,#12557,#12558,#12559,#12560,#12561,#12562,#12563,#12564),
 .UNSPECIFIED.,.F.,.F.,(4,2,2,2,2,2,2,2,2,2,2,2,2,2,2,2,2,2,2,2,2,2,2,2,
2,2,2,2,2,2,2,2,2,2,2,2,2,2,2,2,2,2,2,2,2,4),(-4.06035618685406,-3.99361167849707,
-3.98439999022834,-3.98322214866527,-3.98248341448087,-3.98179268930348,
-3.98123216837419,-3.98058076863918,-3.97946144696294,-3.97526766961926,
-3.90378714042804,-3.89074774847312,-3.8781122663538,-3.84219985006292,
-3.82546256057995,-3.82330259771421,-3.82195579736669,-3.82069809982943,
-3.81978625098544,-3.81881413273403,-3.81715495200595,-3.81264863723276,
-3.74278858558718,-3.71703578795096,-3.68974695454361,-3.66956640223594,
-3.66384816204599,-3.66036248865856,-3.65961238107755,-3.65891347862774,
-3.65835241515155,-3.65770720013465,-3.6566143936515,-3.65267846424478,
-3.58488437228641,-3.53713831131176,-3.50614519376003,-3.50030166824999,
-3.49898555618717,-3.49775003070747,-3.49684099707044,-3.49585916066768,
-3.49444560403126,-3.49049260806214,-3.42563801691695,-3.39969022993959),
 .UNSPECIFIED.);
#83=B_SPLINE_CURVE_WITH_KNOTS('',3,(#12566,#12567,#12568,#12569,#12570,
#12571,#12572,#12573,#12574,#12575,#12576,#12577,#12578,#12579,#12580,#12581,
#12582,#12583,#12584,#12585,#12586,#12587,#12588,#12589,#12590,#12591,#12592,
#12593,#12594,#12595,#12596,#12597,#12598,#12599,#12600,#12601,#12602,#12603,
#12604,#12605,#12606,#12607,#12608,#12609,#12610,#12611,#12612,#12613,#12614,
#12615,#12616,#12617,#12618,#12619,#12620,#12621,#12622,#12623,#12624,#12625,
#12626,#12627,#12628,#12629,#12630,#12631,#12632,#12633,#12634,#12635,#12636,
#12637,#12638,#12639,#12640,#12641,#12642,#12643,#12644,#12645,#12646,#12647,
#12648,#12649,#12650,#12651,#12652,#12653,#12654,#12655),.UNSPECIFIED.,
 .F.,.F.,(4,2,2,2,2,2,2,2,2,2,2,2,2,2,2,2,2,2,2,2,2,2,2,2,2,2,2,2,2,2,2,
2,2,2,2,2,2,2,2,2,2,2,2,2,4),(-0.662566381801328,-0.642307042402579,-0.631927247965306,
-0.630545453535587,-0.629834389016777,-0.629308056282692,-0.628743230621758,
-0.627963160501452,-0.627086856245606,-0.625576482979552,-0.622372085393098,
-0.613477033548835,-0.593317933234046,-0.47687922138088,-0.470865665074005,
-0.469000027277596,-0.467986425240083,-0.466981540872009,-0.465758797128514,
-0.463453519228134,-0.450214186112101,-0.429788140307287,-0.376603389375201,
-0.352555446920475,-0.310102493005206,-0.307662135184486,-0.306840102703051,
-0.306283784139431,-0.305730622929776,-0.305039438187828,-0.303775956894423,
-0.302135288918424,-0.298549825141854,-0.288178350049604,-0.257620541822341,
-0.154107817669735,-0.147874941188741,-0.145983065491394,-0.144964276040553,
-0.143969534392672,-0.142759728502392,-0.140514393987957,-0.128469004090863,
-0.104709114538698,-0.000962379493694885),.UNSPECIFIED.);
#84=B_SPLINE_CURVE_WITH_KNOTS('',3,(#12656,#12657,#12658,#12659,#12660,
#12661,#12662,#12663,#12664,#12665,#12666,#12667,#12668,#12669,#12670,#12671,
#12672,#12673,#12674,#12675,#12676,#12677,#12678,#12679,#12680,#12681,#12682,
#12683,#12684,#12685,#12686,#12687,#12688,#12689,#12690,#12691,#12692,#12693,
#12694,#12695,#12696,#12697,#12698,#12699,#12700,#12701,#12702,#12703,#12704,
#12705,#12706,#12707,#12708,#12709,#12710,#12711,#12712,#12713,#12714,#12715,
#12716,#12717,#12718,#12719,#12720,#12721,#12722,#12723,#12724,#12725,#12726,
#12727,#12728,#12729,#12730,#12731,#12732,#12733,#12734,#12735,#12736,#12737,
#12738,#12739,#12740,#12741,#12742,#12743,#12744,#12745,#12746,#12747,#12748,
#12749,#12750,#12751,#12752,#12753,#12754,#12755,#12756,#12757,#12758,#12759,
#12760,#12761,#12762,#12763,#12764,#12765,#12766,#12767,#12768,#12769,#12770,
#12771,#12772,#12773,#12774,#12775,#12776,#12777,#12778,#12779,#12780,#12781,
#12782,#12783,#12784,#12785,#12786,#12787,#12788,#12789,#12790,#12791,#12792,
#12793,#12794,#12795,#12796,#12797,#12798,#12799,#12800,#12801,#12802,#12803,
#12804,#12805,#12806,#12807,#12808,#12809,#12810,#12811,#12812,#12813,#12814,
#12815,#12816,#12817,#12818,#12819,#12820,#12821,#12822,#12823,#12824,#12825,
#12826,#12827,#12828,#12829,#12830,#12831,#12832,#12833,#12834,#12835,#12836,
#12837,#12838,#12839,#12840,#12841,#12842,#12843,#12844,#12845,#12846,#12847,
#12848,#12849,#12850,#12851,#12852,#12853,#12854,#12855,#12856,#12857,#12858,
#12859,#12860,#12861,#12862,#12863,#12864,#12865,#12866,#12867,#12868,#12869,
#12870,#12871),.UNSPECIFIED.,.F.,.F.,(4,2,2,2,2,2,2,2,2,2,2,2,2,2,2,2,2,
2,2,2,2,2,2,2,2,2,2,2,2,2,2,2,2,2,2,2,2,2,2,2,2,2,2,2,2,2,2,2,2,2,2,2,2,
2,2,2,2,2,2,2,2,2,2,2,2,2,2,2,2,2,2,2,2,2,2,2,2,2,2,2,2,2,2,2,2,2,2,2,2,
2,2,2,2,2,2,2,2,2,2,2,2,2,2,2,2,2,2,4),(-4.06047319610046,-4.04534584298061,
-4.04416539400911,-4.04342571802198,-4.04286616394116,-4.04233217020568,
-4.04180297221772,-4.04107932890953,-4.03964705149221,-4.02786985803002,
-4.0262296518368,-4.02273295415447,-3.93530219498073,-3.90496108430936,
-3.88551862057472,-3.88298665323852,-3.88171726745532,-3.88080428751781,
-3.87983778136405,-3.87847870528836,-3.87567072018144,-3.84597591307066,
-3.75834525501736,-3.74511926195674,-3.72942328193803,-3.72446010513923,
-3.7223747566678,-3.72127184208784,-3.72033338154978,-3.71973421294788,
-3.71917838645758,-3.71843917992707,-3.71720182332762,-3.70991742469021,
-3.65693198605897,-3.65171157372666,-3.64580315825785,-3.63901498916356,
-3.63106046243552,-3.62145481653966,-3.56675865525092,-3.56134919016542,
-3.5596294281448,-3.55853631809543,-3.55751883756009,-3.55619796928395,
-3.55333293238161,-3.53181712534797,-3.51438522036448,-3.51335591294048,
-3.43487651601576,-3.42175414833139,-3.40648152019466,-3.40167102851742,
-3.39963319065503,-3.39854848198509,-3.39784895002736,-3.39722245491491,
-3.39667359783532,-3.39610292231898,-3.39503112368044,-3.3913990297126,
-3.39034561572905,-3.30815746727068,-3.29739957779183,-3.28438570763044,
-3.25393966719276,-3.23973628797277,-3.23738856875607,-3.23615732533456,
-3.23515261322027,-3.2341452008143,-3.23230811804009,-3.22651846056045,
-3.10872130567222,-3.08564326288441,-3.07945647921663,-3.07700285920929,
-3.07576136466618,-3.07499607997045,-3.07431450390968,-3.07376151595188,
-3.07321463287533,-3.07226141163202,-3.06955450193642,-3.02624149133466,
-3.00985954781861,-2.96046465672555,-2.91803799525615,-2.91486242600556,
-2.91346939124196,-2.91244353904541,-2.91149600520922,-2.91021004927341,
-2.90769439567261,-2.88798357653557,-2.88168747283358,-2.80433381257472,
-2.75603059941067,-2.75390269102062,-2.75278338950051,-2.7520692484402,
-2.75140592379423,-2.75085691570476,-2.75028550288771,-2.74921062600865,
-2.7455534977854,-2.6924050095202),.UNSPECIFIED.);
#85=B_SPLINE_CURVE_WITH_KNOTS('',3,(#12876,#12877,#12878,#12879,#12880,
#12881,#12882,#12883,#12884,#12885,#12886,#12887,#12888,#12889,#12890,#12891,
#12892,#12893,#12894,#12895,#12896,#12897,#12898,#12899,#12900,#12901,#12902,
#12903,#12904,#12905,#12906,#12907,#12908,#12909,#12910,#12911,#12912,#12913,
#12914,#12915,#12916,#12917,#12918,#12919,#12920,#12921,#12922,#12923,#12924,
#12925,#12926,#12927,#12928,#12929,#12930,#12931,#12932,#12933,#12934,#12935,
#12936,#12937,#12938,#12939,#12940,#12941,#12942,#12943,#12944,#12945,#12946,
#12947,#12948,#12949,#12950,#12951,#12952,#12953,#12954,#12955,#12956,#12957,
#12958,#12959,#12960,#12961,#12962,#12963,#12964,#12965,#12966,#12967,#12968,
#12969,#12970,#12971,#12972,#12973,#12974,#12975,#12976,#12977,#12978,#12979,
#12980,#12981,#12982,#12983,#12984,#12985,#12986,#12987,#12988,#12989,#12990,
#12991,#12992,#12993,#12994,#12995,#12996,#12997,#12998,#12999,#13000,#13001,
#13002,#13003,#13004,#13005,#13006,#13007,#13008,#13009,#13010,#13011,#13012,
#13013,#13014,#13015,#13016,#13017,#13018,#13019,#13020,#13021,#13022,#13023,
#13024,#13025,#13026,#13027,#13028,#13029,#13030,#13031,#13032,#13033,#13034,
#13035,#13036,#13037,#13038,#13039,#13040,#13041,#13042,#13043,#13044,#13045,
#13046,#13047,#13048,#13049,#13050,#13051,#13052,#13053,#13054,#13055,#13056,
#13057,#13058,#13059,#13060,#13061,#13062,#13063,#13064,#13065,#13066,#13067,
#13068,#13069,#13070,#13071,#13072,#13073,#13074,#13075,#13076,#13077,#13078,
#13079,#13080,#13081,#13082,#13083,#13084,#13085,#13086,#13087,#13088,#13089,
#13090,#13091,#13092,#13093,#13094,#13095,#13096,#13097,#13098,#13099,#13100,
#13101,#13102,#13103,#13104,#13105,#13106,#13107,#13108,#13109,#13110,#13111,
#13112,#13113,#13114,#13115,#13116,#13117,#13118,#13119,#13120,#13121,#13122,
#13123,#13124,#13125,#13126,#13127,#13128,#13129,#13130,#13131,#13132,#13133,
#13134,#13135,#13136,#13137,#13138,#13139,#13140,#13141,#13142,#13143,#13144,
#13145,#13146,#13147,#13148,#13149,#13150,#13151,#13152,#13153,#13154,#13155,
#13156,#13157,#13158,#13159,#13160,#13161,#13162,#13163,#13164,#13165,#13166,
#13167),.UNSPECIFIED.,.F.,.F.,(4,2,2,2,2,2,2,2,2,2,2,2,2,2,2,2,2,2,2,2,
2,2,2,2,2,2,2,2,2,2,2,2,2,2,2,2,2,2,2,2,2,2,2,2,2,2,2,2,2,2,2,2,2,2,2,2,
2,2,2,2,2,2,2,2,2,2,2,2,2,2,2,2,2,2,2,2,2,2,2,2,2,2,2,2,2,2,2,2,2,2,2,2,
2,2,2,2,2,2,2,2,2,2,2,2,2,2,2,2,2,2,2,2,2,2,2,2,2,2,2,2,2,2,2,2,2,2,2,2,
2,2,2,2,2,2,2,2,2,2,2,2,2,2,2,2,2,4),(-3.39963798704962,-3.3801463624031,
-3.33503323920271,-3.31747483966743,-3.31498860782002,-3.31372820042422,
-3.31281609888343,-3.31184531483645,-3.3101923769096,-3.30572577982014,
-3.23578479200766,-3.19718455641332,-3.16541403173404,-3.15412338052256,
-3.15270150731027,-3.15212963486832,-3.15155394251863,-3.15102749152131,
-3.15031520774104,-3.14892793874885,-3.13839446348343,-3.1365083456454,
-3.1355832342568,-3.13412120005603,-3.11027876147053,-3.04140611119487,
-3.00000319293854,-2.99348740885993,-2.99164549279878,-2.9905248184623,
-2.98951462919597,-2.98822681126885,-2.98560567867272,-2.9773442356549,
-2.97586363935894,-2.97448427771589,-2.97213428695755,-2.97007180630593,
-2.96835338791431,-2.96715148591709,-2.9654647030675,-2.95822543174843,
-2.93329148827552,-2.88200765458009,-2.83254193996605,-2.83027173378525,
-2.82941336621256,-2.82882263855469,-2.82824911811561,-2.82755714495274,
-2.82582678866122,-2.80983706645041,-2.8028903314239,-2.72639022844628,
-2.68792343573436,-2.67171269761921,-2.66927301641488,-2.66802226850856,
-2.66711149323465,-2.66613677203362,-2.66474860313483,-2.6609612565459,
-2.60026563696323,-2.51140709835283,-2.50893300242785,-2.50712520641222,
-2.50634488924346,-2.50577010993714,-2.5052424755221,-2.50452567253001,
-2.50312096632339,-2.49213091847282,-2.49109047059713,-2.40545604696581,
-2.35100639651447,-2.34697619345248,-2.34544191327064,-2.3443886510429,
-2.34335972021447,-2.34212329769835,-2.33905431486547,-2.31127975027033,
-2.2217148279477,-2.18601475110079,-2.18412392317036,-2.1833267571815,-2.18275181345288,
-2.18222432256387,-2.18150814089206,-2.18010591665074,-2.16918354718316,
-2.1658631395019,-2.16545353103077,-2.16263341147185,-2.1608514978219,-2.15902128399188,
-2.12316188851408,-2.07229719421697,-2.03118377265546,-2.02482385120089,
-2.02291701539089,-2.02178167954957,-2.02087468505537,-2.01965817915969,
-2.01738162394926,-2.00472874048174,-1.97995857104196,-1.89085274533575,
-1.86319994536807,-1.86126286456821,-1.86051658610009,-1.85998118146519,
-1.85941161750617,-1.85864563128774,-1.85693088564842,-1.81478627941541,
-1.7621476763672,-1.70487425613477,-1.70108226061158,-1.69969310680157,
-1.69871791772339,-1.69780688383685,-1.69655605759408,-1.69433108046041,
-1.69146228328892,-1.67054178538779,-1.64795565705583,-1.56603769255167,
-1.54017868939998,-1.53827039839572,-1.53752885577601,-1.53699468089012,
-1.53642431052022,-1.53565368344678,-1.53406491830582,-1.52042369118033,
-1.49436519595056,-1.4161911279273,-1.38099170084747,-1.37780306017645,
-1.37651298043796,-1.37556413751083,-1.37453852831644,-1.37314876494592,
-1.37006446976188,-1.3700182626362),.UNSPECIFIED.);
#86=B_SPLINE_CURVE_WITH_KNOTS('',3,(#13168,#13169,#13170,#13171,#13172,
#13173,#13174,#13175,#13176,#13177,#13178,#13179,#13180,#13181,#13182,#13183,
#13184,#13185,#13186,#13187,#13188,#13189,#13190,#13191,#13192,#13193,#13194,
#13195,#13196,#13197,#13198,#13199,#13200,#13201,#13202,#13203,#13204,#13205,
#13206,#13207,#13208,#13209,#13210,#13211,#13212,#13213,#13214,#13215,#13216,
#13217,#13218,#13219,#13220,#13221,#13222,#13223,#13224,#13225,#13226,#13227,
#13228,#13229,#13230,#13231,#13232,#13233,#13234,#13235,#13236,#13237,#13238,
#13239,#13240,#13241,#13242,#13243,#13244,#13245,#13246,#13247,#13248,#13249,
#13250,#13251,#13252,#13253,#13254,#13255,#13256,#13257,#13258,#13259,#13260,
#13261,#13262,#13263,#13264,#13265,#13266,#13267,#13268,#13269,#13270,#13271,
#13272,#13273,#13274,#13275,#13276,#13277,#13278,#13279,#13280,#13281,#13282,
#13283,#13284,#13285,#13286,#13287,#13288,#13289,#13290,#13291,#13292,#13293,
#13294,#13295,#13296,#13297,#13298,#13299,#13300,#13301,#13302,#13303,#13304,
#13305,#13306,#13307,#13308,#13309,#13310,#13311,#13312,#13313,#13314,#13315,
#13316,#13317,#13318,#13319,#13320,#13321,#13322,#13323,#13324,#13325,#13326,
#13327,#13328,#13329,#13330,#13331,#13332,#13333,#13334,#13335,#13336,#13337,
#13338,#13339,#13340,#13341,#13342,#13343,#13344,#13345,#13346,#13347,#13348,
#13349,#13350,#13351,#13352,#13353,#13354,#13355,#13356,#13357,#13358,#13359,
#13360,#13361,#13362,#13363,#13364,#13365,#13366,#13367,#13368,#13369,#13370,
#13371,#13372,#13373,#13374,#13375,#13376,#13377,#13378,#13379,#13380,#13381,
#13382,#13383,#13384,#13385,#13386,#13387,#13388,#13389,#13390,#13391,#13392,
#13393,#13394,#13395,#13396,#13397,#13398,#13399,#13400,#13401,#13402,#13403,
#13404,#13405,#13406,#13407,#13408,#13409,#13410,#13411,#13412,#13413,#13414,
#13415,#13416,#13417,#13418,#13419,#13420,#13421,#13422,#13423,#13424,#13425,
#13426,#13427,#13428,#13429,#13430,#13431,#13432,#13433,#13434,#13435),
 .UNSPECIFIED.,.F.,.F.,(4,2,2,2,2,2,2,2,2,2,2,2,2,2,2,2,2,2,2,2,2,2,2,2,
2,2,2,2,2,2,2,2,2,2,2,2,2,2,2,2,2,2,2,2,2,2,2,2,2,2,2,2,2,2,2,2,2,2,2,2,
2,2,2,2,2,2,2,2,2,2,2,2,2,2,2,2,2,2,2,2,2,2,2,2,2,2,2,2,2,2,2,2,2,2,2,2,
2,2,2,2,2,2,2,2,2,2,2,2,2,2,2,2,2,2,2,2,2,2,2,2,2,2,2,2,2,2,2,2,2,2,2,2,
2,4),(-2.6924050095202,-2.68642891308495,-2.64342279511557,-2.60911170960607,
-2.59398314520964,-2.5915962610922,-2.5903564984864,-2.5893508801732,-2.5883475873379,
-2.5865321228209,-2.58091462116684,-2.48819071299198,-2.43336099519159,
-2.43109790870853,-2.42992737528862,-2.42919171106608,-2.42851294842858,
-2.42796299827926,-2.42731748260204,-2.42622333824083,-2.42227452987842,
-2.35808439070906,-2.33325900814762,-2.30428544406198,-2.27504080974453,
-2.2697836267792,-2.26808174249944,-2.26699221143255,-2.2659725753604,-2.26464106510559,
-2.26182857348486,-2.24077454455778,-2.23828694620631,-2.22172473220441,
-2.13832501443953,-2.11664611819253,-2.10766753253107,-2.10631461940788,
-2.10561942724472,-2.10505858878972,-2.10441054397551,-2.10330574668048,
-2.09925544159485,-2.03172869249018,-1.95195643851913,-1.94685995131592,
-1.94511457370892,-1.94412527893165,-1.94321788528285,-1.94199738915162,
-1.9397021457465,-1.92666792358696,-1.90254407047974,-1.81458824953252,
-1.80700198628684,-1.79811745036071,-1.79762434913496,-1.79680812683313,
-1.78500867117236,-1.78357487636116,-1.7828505835689,-1.78232096597438,
-1.78174759439861,-1.78095937424306,-1.77912044841993,-1.73401008824978,
-1.63026584462984,-1.62402675192692,-1.62213417783524,-1.62111526929572,
-1.6201868888682,-1.61904718632739,-1.61782195897111,-1.61595046703596,
-1.61250012800757,-1.58381013371298,-1.54061546022415,-1.46562662399494,
-1.46511055584924,-1.46113603254543,-1.46003913909064,-1.45939295372624,
-1.45883196278505,-1.45813432692258,-1.45676958414006,-1.44746566983231,
-1.42445685182236,-1.30655372447723,-1.30077308952915,-1.29893680009627,
-1.29792935119908,-1.29694439517905,-1.29574603455664,-1.29445773953861,
-1.29243651969806,-1.28859980192737,-1.25434760256718,-1.15940771580721,
-1.1555336512672,-1.1545735800796,-1.13892822369334,-1.13720757342173,-1.13651714760256,
-1.1359439873102,-1.13535263347187,-1.13447392429836,-1.13206489299596,
-1.09284674087391,-0.983821308633121,-0.977721682838613,-0.975846038465802,
-0.974830673799416,-0.973846436504311,-0.972662332388304,-0.971392381494991,
-0.969414633580607,-0.965690836890829,-0.933100508755005,-0.844865441353235,
-0.834999250179034,-0.833101662099482,-0.831773057111843,-0.815851704052827,
-0.814123258818844,-0.813431583065616,-0.812858125965805,-0.812267264778896,
-0.81139072582339,-0.808996437677532,-0.770749363486924,-0.758866562162959,
-0.74889831689786,-0.687082703388265,-0.662225552500327),.UNSPECIFIED.);
#87=B_SPLINE_CURVE_WITH_KNOTS('',3,(#13441,#13442,#13443,#13444,#13445,
#13446,#13447,#13448,#13449,#13450,#13451,#13452,#13453,#13454,#13455,#13456,
#13457,#13458,#13459,#13460,#13461,#13462,#13463,#13464,#13465,#13466,#13467,
#13468,#13469,#13470,#13471,#13472,#13473,#13474,#13475,#13476,#13477,#13478,
#13479,#13480,#13481,#13482,#13483,#13484,#13485,#13486,#13487,#13488,#13489,
#13490,#13491,#13492,#13493,#13494,#13495,#13496,#13497,#13498,#13499,#13500,
#13501,#13502,#13503,#13504,#13505,#13506,#13507,#13508,#13509,#13510,#13511,
#13512,#13513,#13514,#13515,#13516,#13517,#13518,#13519,#13520,#13521,#13522,
#13523,#13524,#13525,#13526,#13527,#13528,#13529,#13530,#13531,#13532,#13533,
#13534,#13535,#13536,#13537,#13538,#13539,#13540,#13541,#13542,#13543,#13544,
#13545,#13546,#13547,#13548,#13549,#13550,#13551,#13552,#13553,#13554,#13555,
#13556,#13557,#13558,#13559,#13560,#13561,#13562,#13563,#13564,#13565,#13566,
#13567,#13568,#13569,#13570,#13571,#13572,#13573,#13574,#13575,#13576,#13577,
#13578,#13579,#13580,#13581,#13582,#13583,#13584,#13585,#13586,#13587,#13588,
#13589,#13590,#13591,#13592,#13593,#13594,#13595,#13596,#13597,#13598,#13599,
#13600,#13601,#13602,#13603,#13604,#13605,#13606,#13607,#13608,#13609,#13610,
#13611,#13612,#13613,#13614,#13615,#13616,#13617,#13618,#13619,#13620,#13621,
#13622,#13623,#13624,#13625,#13626,#13627,#13628,#13629,#13630,#13631,#13632,
#13633,#13634,#13635,#13636,#13637,#13638,#13639,#13640,#13641,#13642,#13643,
#13644,#13645,#13646,#13647,#13648,#13649,#13650,#13651,#13652,#13653,#13654,
#13655,#13656,#13657,#13658,#13659,#13660,#13661,#13662,#13663,#13664,#13665,
#13666,#13667,#13668,#13669,#13670),.UNSPECIFIED.,.F.,.F.,(4,2,2,2,2,2,
2,2,2,2,2,2,2,2,2,2,2,2,2,2,2,2,2,2,2,2,2,2,2,2,2,2,2,2,2,2,2,2,2,2,2,2,
2,2,2,2,2,2,2,2,2,2,2,2,2,2,2,2,2,2,2,2,2,2,2,2,2,2,2,2,2,2,2,2,2,2,2,2,
2,2,2,2,2,2,2,2,2,2,2,2,2,2,2,2,2,2,2,2,2,2,2,2,2,2,2,2,2,2,2,2,2,2,2,2,
4),(-1.36933580029482,-1.36685434590888,-1.36489436748477,-1.35480597029584,
-1.35328431549134,-1.3525627033398,-1.35199784247543,-1.35137369114127,
-1.35036769919804,-1.34691195881337,-1.32465236042517,-1.25872574888066,
-1.19709907076041,-1.19331180451753,-1.19192329337445,-1.19094821534783,
-1.19003701479565,-1.18878553999599,-1.18634394507964,-1.17007358821919,
-1.13138876938743,-1.06590527017317,-1.05302557088158,-1.0506948760313,
-1.04925113861638,-1.04715896223443,-1.04631814496416,-1.04591121633372,
-1.0451413396503,-1.04440053621934,-1.04311229353906,-1.03188745467814,
-1.03031738950424,-1.02958648241428,-1.02902031422942,-1.02840095652667,
-1.02741593142817,-1.02416366506071,-1.01893919292446,-1.00541698416013,
-0.974196927855472,-0.932524209166809,-0.874216467908195,-0.870382552085268,
-0.868986838394231,-0.868009763794535,-0.867099121419448,-0.865852160241502,
-0.863432359506044,-0.849122318907712,-0.830666780537513,-0.79029497564326,
-0.748728636782336,-0.71809664715751,-0.716809030995085,-0.715305151953588,
-0.712529953720571,-0.708262431568275,-0.707135605047334,-0.70648236059627,
-0.705921812086907,-0.705383324993881,-0.704287162729645,-0.699881061533425,
-0.692083071464235,-0.67272299237665,-0.633143989027252,-0.552940401187442,
-0.547830955348225,-0.546083555098341,-0.545093722574369,-0.544186206801683,
-0.542966098823524,-0.540673383588316,-0.527947292407187,-0.495752375365148,
-0.487868121601157,-0.481545700416331,-0.43852589759176,-0.402500153446669,
-0.386264157382296,-0.384699329270653,-0.383942292282003,-0.383403977149381,
-0.382892781691509,-0.382344655882414,-0.381638936574097,-0.378789560123842,
-0.37438776330426,-0.360698708546912,-0.337609289557772,-0.317116640240227,
-0.285708452326109,-0.228315541179422,-0.22451663837901,-0.223126351679466,
-0.222150802348841,-0.221239777422601,-0.21998949920154,-0.21755356641792,
-0.202477368397074,-0.153312818696664,-0.136544937420956,-0.128280902080467,
-0.119063008784389,-0.0749051582841398,-0.0631519213070257,-0.0615814607740693,
-0.0608392917967397,-0.0602714293384798,-0.0596574167597624,-0.059026908384464,
-0.0581076872292814,-0.056491098985421,-0.000961071678187754),
 .UNSPECIFIED.);
#88=B_SPLINE_CURVE_WITH_KNOTS('',3,(#13671,#13672,#13673,#13674,#13675,
#13676,#13677,#13678,#13679,#13680,#13681,#13682,#13683,#13684,#13685,#13686,
#13687,#13688,#13689,#13690,#13691,#13692,#13693,#13694,#13695,#13696,#13697,
#13698,#13699,#13700,#13701,#13702,#13703,#13704,#13705,#13706,#13707,#13708,
#13709,#13710,#13711,#13712,#13713,#13714,#13715,#13716,#13717,#13718,#13719,
#13720,#13721,#13722,#13723,#13724,#13725,#13726,#13727,#13728,#13729,#13730,
#13731,#13732,#13733,#13734,#13735,#13736,#13737,#13738,#13739,#13740,#13741,
#13742,#13743,#13744,#13745,#13746,#13747,#13748,#13749,#13750,#13751,#13752,
#13753,#13754,#13755,#13756,#13757,#13758,#13759,#13760),.UNSPECIFIED.,
 .F.,.F.,(4,2,2,2,2,2,2,2,2,2,2,2,2,2,2,2,2,2,2,2,2,2,2,2,2,2,2,2,2,2,2,
2,2,2,2,2,2,2,2,2,2,2,2,2,4),(-4.06081080818158,-3.97254646944807,-3.96598950378341,
-3.96298913079805,-3.96059351635776,-3.95935201078245,-3.9583463749307,
-3.95734422127451,-3.95553403847313,-3.94995623461136,-3.85805141253993,
-3.83816751636306,-3.81202015485741,-3.79979020396287,-3.79875902822199,
-3.79808190059324,-3.79754275723518,-3.79703610009293,-3.7964848361183,
-3.79550986711415,-3.79265100789042,-3.74366436221132,-3.71970253130055,
-3.69647514053989,-3.65675031186624,-3.64021162345936,-3.63776051829344,
-3.6365073688447,-3.63559624731789,-3.63462248064216,-3.63323788429951,
-3.62947380489197,-3.57261200094989,-3.54162896394138,-3.50239471556971,
-3.47853849129411,-3.47599500762396,-3.47531398579534,-3.47477369631238,
-3.4742665248669,-3.47371730766684,-3.47275256641134,-3.46996415707241,
-3.42646651277619,-3.39963798704962),.UNSPECIFIED.);
#89=B_SPLINE_CURVE_WITH_KNOTS('',3,(#13762,#13763,#13764,#13765,#13766,
#13767,#13768,#13769,#13770,#13771,#13772,#13773,#13774,#13775,#13776,#13777,
#13778,#13779,#13780,#13781,#13782,#13783,#13784,#13785,#13786,#13787,#13788,
#13789,#13790,#13791,#13792,#13793,#13794,#13795,#13796,#13797,#13798,#13799,
#13800,#13801,#13802,#13803,#13804,#13805,#13806,#13807,#13808,#13809,#13810,
#13811,#13812,#13813,#13814,#13815,#13816,#13817,#13818,#13819,#13820,#13821,
#13822,#13823,#13824,#13825,#13826,#13827,#13828,#13829,#13830,#13831,#13832,
#13833,#13834,#13835,#13836,#13837,#13838,#13839,#13840,#13841,#13842,#13843,
#13844,#13845,#13846,#13847,#13848,#13849,#13850,#13851,#13852,#13853,#13854,
#13855,#13856,#13857,#13858,#13859,#13860,#13861,#13862,#13863,#13864,#13865,
#13866,#13867,#13868,#13869,#13870,#13871),.UNSPECIFIED.,.F.,.F.,(4,2,2,
2,2,2,2,2,2,2,2,2,2,2,2,2,2,2,2,2,2,2,2,2,2,2,2,2,2,2,2,2,2,2,2,2,2,2,2,
2,2,2,2,2,2,2,2,2,2,2,2,2,2,2,4),(-0.662225552500327,-0.656915475901761,
-0.654094279685166,-0.652731584139461,-0.651763761058461,-0.650769380826292,
-0.649484912821886,-0.648077451830496,-0.645772576183879,-0.607416192165025,
-0.509195274519436,-0.508993483768699,-0.507062659781684,-0.506699670647006,
-0.505795926386445,-0.505322534985358,-0.504525025115455,-0.492702146991682,
-0.49126760132188,-0.490543137750809,-0.490013495181177,-0.489440197184266,
-0.488652252520684,-0.486814750144522,-0.442009704914305,-0.418914184542673,
-0.390121669982303,-0.334541928051994,-0.331059469460802,-0.329719800275287,
-0.328758040194021,-0.327760691969241,-0.32645741569573,-0.325023968814133,
-0.322657030438605,-0.276333688584542,-0.173374216379223,-0.172657714031728,
-0.168830077812296,-0.16773580740683,-0.167160321233803,-0.1666561992001,
-0.16600249409107,-0.164843360661631,-0.159645732572176,-0.105976682679097,
-0.0344455005358403,-0.0131096786969769,-0.0083810641565655,-0.00668827843886096,
-0.00570931015307833,-0.00472820051572089,-0.0037516187691957,-0.00214249435605951,
-0.000961424493519781),.UNSPECIFIED.);
#90=B_SPLINE_CURVE_WITH_KNOTS('',3,(#13872,#13873,#13874,#13875,#13876,
#13877,#13878,#13879,#13880,#13881,#13882,#13883,#13884,#13885,#13886,#13887,
#13888,#13889,#13890,#13891,#13892,#13893,#13894,#13895,#13896,#13897,#13898,
#13899,#13900,#13901,#13902,#13903,#13904,#13905,#13906,#13907,#13908,#13909,
#13910,#13911,#13912,#13913,#13914,#13915,#13916,#13917,#13918,#13919,#13920,
#13921,#13922,#13923,#13924,#13925,#13926,#13927,#13928,#13929,#13930,#13931,
#13932,#13933,#13934,#13935,#13936,#13937,#13938,#13939,#13940,#13941,#13942,
#13943,#13944,#13945,#13946,#13947,#13948,#13949,#13950,#13951,#13952,#13953,
#13954,#13955,#13956,#13957,#13958,#13959,#13960,#13961,#13962,#13963,#13964,
#13965,#13966,#13967,#13968,#13969,#13970,#13971,#13972,#13973,#13974,#13975,
#13976,#13977,#13978,#13979,#13980,#13981,#13982,#13983,#13984,#13985,#13986,
#13987,#13988,#13989,#13990,#13991,#13992,#13993,#13994,#13995,#13996,#13997,
#13998,#13999,#14000,#14001,#14002,#14003,#14004,#14005,#14006,#14007,#14008,
#14009,#14010,#14011,#14012,#14013,#14014,#14015,#14016,#14017,#14018,#14019,
#14020,#14021,#14022,#14023,#14024,#14025,#14026,#14027,#14028,#14029,#14030,
#14031,#14032,#14033,#14034,#14035,#14036,#14037,#14038,#14039,#14040,#14041,
#14042,#14043),.UNSPECIFIED.,.F.,.F.,(4,2,2,2,2,2,2,2,2,2,2,2,2,2,2,2,2,
2,2,2,2,2,2,2,2,2,2,2,2,2,2,2,2,2,2,2,2,2,2,2,2,2,2,2,2,2,2,2,2,2,2,2,2,
2,2,2,2,2,2,2,2,2,2,2,2,2,2,2,2,2,2,2,2,2,2,2,2,2,2,2,2,2,2,2,2,4),(-4.06144638480364,
-4.05919065566942,-4.05240797511435,-3.95307084923477,-3.91100322525023,
-3.90626966855807,-3.90514515424867,-3.9044991495446,-3.9039380295739,-3.90323986657943,
-3.90216435092963,-3.89732232099656,-3.80722477802761,-3.76990221440686,
-3.75486044676713,-3.74636537497466,-3.74490620736317,-3.74358422074853,
-3.74258382916825,-3.74162763243638,-3.74030911630387,-3.73695406553281,
-3.69242830353027,-3.64226878304747,-3.5884916767847,-3.58332682229674,
-3.58217014215797,-3.58151704059188,-3.58101300797117,-3.58043721918569,
-3.57934116056596,-3.57549624057306,-3.57480496710874,-3.47182663685071,
-3.4295773122845,-3.42298330110116,-3.42162708554947,-3.42037954516056,
-3.41939014538462,-3.4184075240817,-3.41699122507982,-3.41301988914435,
-3.34837077914238,-3.30192778344226,-3.26121341061206,-3.25946289062047,
-3.25869043566116,-3.25811983883966,-3.25758629563526,-3.25684690632901,
-3.25535314513071,-3.24169502201747,-3.24097321767489,-3.23642293525557,
-3.22647997778993,-3.14395608015912,-3.1061319003723,-3.09996078234044,
-3.0986312201838,-3.09740300637273,-3.0964158872732,-3.09528045882963,-3.09345145010086,
-3.08743065874654,-2.97142865816801,-2.94710271775015,-2.93747541316192,
-2.9360991743505,-2.93539907398724,-2.93483779561794,-2.93427646322084,
-2.93325228912262,-2.93002026140098,-2.87469654985874,-2.82404422793751,
-2.8022728656313,-2.78620986520908,-2.77728541406992,-2.77580607264692,
-2.7744695323233,-2.77346665202304,-2.77251440473491,-2.77121127070329,
-2.76794725507986,-2.76576455985351,-2.6922410793174),.UNSPECIFIED.);
#91=B_SPLINE_CURVE_WITH_KNOTS('',3,(#14048,#14049,#14050,#14051,#14052,
#14053,#14054,#14055,#14056,#14057,#14058,#14059,#14060,#14061,#14062,#14063,
#14064,#14065,#14066,#14067,#14068,#14069,#14070,#14071,#14072,#14073,#14074,
#14075,#14076,#14077,#14078,#14079,#14080,#14081,#14082,#14083,#14084,#14085,
#14086,#14087,#14088,#14089,#14090,#14091,#14092,#14093,#14094,#14095,#14096,
#14097,#14098,#14099,#14100,#14101,#14102,#14103,#14104,#14105,#14106,#14107,
#14108,#14109,#14110,#14111,#14112,#14113,#14114,#14115,#14116,#14117,#14118,
#14119,#14120,#14121,#14122,#14123,#14124,#14125,#14126,#14127,#14128,#14129,
#14130,#14131,#14132,#14133,#14134,#14135,#14136,#14137,#14138,#14139,#14140,
#14141,#14142,#14143,#14144,#14145,#14146,#14147,#14148,#14149,#14150,#14151,
#14152,#14153,#14154,#14155,#14156,#14157,#14158,#14159,#14160,#14161,#14162,
#14163,#14164,#14165,#14166,#14167,#14168,#14169,#14170,#14171,#14172,#14173,
#14174,#14175,#14176,#14177,#14178,#14179,#14180,#14181,#14182,#14183,#14184,
#14185,#14186,#14187,#14188,#14189,#14190,#14191,#14192,#14193,#14194,#14195,
#14196,#14197,#14198,#14199,#14200,#14201,#14202,#14203,#14204,#14205,#14206,
#14207,#14208,#14209,#14210,#14211,#14212,#14213,#14214,#14215,#14216,#14217,
#14218,#14219,#14220,#14221,#14222,#14223,#14224,#14225,#14226,#14227,#14228,
#14229,#14230,#14231,#14232,#14233,#14234,#14235,#14236,#14237,#14238,#14239,
#14240,#14241,#14242,#14243,#14244,#14245,#14246,#14247,#14248,#14249,#14250,
#14251,#14252,#14253,#14254,#14255,#14256,#14257,#14258,#14259,#14260,#14261,
#14262,#14263,#14264,#14265,#14266,#14267,#14268,#14269,#14270,#14271,#14272,
#14273,#14274,#14275,#14276,#14277,#14278,#14279,#14280,#14281,#14282,#14283,
#14284,#14285,#14286,#14287,#14288,#14289,#14290,#14291,#14292,#14293,#14294,
#14295,#14296,#14297,#14298,#14299,#14300,#14301,#14302,#14303,#14304,#14305,
#14306,#14307,#14308,#14309,#14310,#14311,#14312,#14313,#14314,#14315,#14316,
#14317,#14318,#14319),.UNSPECIFIED.,.F.,.F.,(4,2,2,2,2,2,2,2,2,2,2,2,2,
2,2,2,2,2,2,2,2,2,2,2,2,2,2,2,2,2,2,2,2,2,2,2,2,2,2,2,2,2,2,2,2,2,2,2,2,
2,2,2,2,2,2,2,2,2,2,2,2,2,2,2,2,2,2,2,2,2,2,2,2,2,2,2,2,2,2,2,2,2,2,2,2,
2,2,2,2,2,2,2,2,2,2,2,2,2,2,2,2,2,2,2,2,2,2,2,2,2,2,2,2,2,2,2,2,2,2,2,2,
2,2,2,2,2,2,2,2,2,2,2,2,2,2,4),(-3.3998905608284,-3.36728512983728,-3.3165216220863,
-3.29570632376686,-3.29237695365769,-3.29138239889647,-3.29076545694202,
-3.29019859875152,-3.28946284154685,-3.28786700497707,-3.27598056772875,
-3.23198105457235,-3.18076690676289,-3.15238114038521,-3.13998197611609,
-3.13516108703912,-3.13277135392944,-3.13132835682328,-3.13006799864135,
-3.12906467308018,-3.12811325689239,-3.12681322208736,-3.12356706488969,
-3.0855108628911,-3.02936706775133,-2.9744847644014,-2.96970572635586,-2.96857766105995,
-2.96793086156635,-2.96736980881946,-2.96667270043273,-2.96560059202097,
-2.96080073717221,-2.87355072079388,-2.81239917000519,-2.80987572896211,
-2.80781582597809,-2.80665261889776,-2.80571970314026,-2.80470291168966,
-2.80282144819128,-2.79667725886823,-2.68911732543282,-2.66174267098193,
-2.64710249109855,-2.64559839026613,-2.64487240022135,-2.64436081871292,
-2.64382311078167,-2.64306850486718,-2.6410803078615,-2.60987299144671,
-2.5665066275203,-2.52174437638913,-2.49143691183562,-2.48787073890102,
-2.48595376388476,-2.48430629344025,-2.48323828799571,-2.48221827430095,
-2.48088630108514,-2.47807294162079,-2.45701599986302,-2.45471210149877,
-2.445019818415,-2.36282815790668,-2.3413564855565,-2.33174645977177,-2.32378480571599,
-2.32247247876214,-2.321785647723,-2.32127927532706,-2.32072487587035,-2.3197354266716,
-2.31677039913419,-2.31462818929304,-2.22872147501193,-2.18192664339179,
-2.16430705711538,-2.16182893207435,-2.16056979431106,-2.15965746997792,
-2.15868537829655,-2.15730807998916,-2.15359343388215,-2.15215529351109,
-2.07939411929984,-2.03049674697944,-2.02021791334108,-2.01765418671469,
-2.00133669964159,-1.99976965660553,-1.9990119964218,-1.99847344097666,
-1.99796219088357,-1.99723848147826,-1.99574604504187,-1.98170403922362,
-1.95507862560463,-1.84740260657027,-1.84595560832858,-1.84000167342805,
-1.83814327200301,-1.83713108216853,-1.83612600059368,-1.8349007012432,
-1.8325836561893,-1.81909510120922,-1.80058279614118,-1.7592247357299,-1.70323561741335,
-1.69832449905212,-1.69408189729303,-1.67817944339364,-1.67645107467533,
-1.67575926478383,-1.67518563150524,-1.67459451913173,-1.67373535088149,
-1.67144523440998,-1.62052436010717,-1.53977960825839,-1.5186843633618,
-1.51611832414237,-1.51481920601549,-1.51386804504227,-1.51284405677621,
-1.51146373831998,-1.50836035977558,-1.49011983684336,-1.4606238808476,
-1.37642590569432,-1.37376626747478,-1.37226986844979,-1.3702919615779,
-1.36933580029482),.UNSPECIFIED.);
#92=B_SPLINE_CURVE_WITH_KNOTS('',3,(#14320,#14321,#14322,#14323,#14324,
#14325,#14326,#14327,#14328,#14329,#14330,#14331,#14332,#14333,#14334,#14335,
#14336,#14337,#14338,#14339,#14340,#14341,#14342,#14343,#14344,#14345,#14346,
#14347,#14348,#14349,#14350,#14351,#14352,#14353,#14354,#14355,#14356,#14357,
#14358,#14359,#14360,#14361,#14362,#14363,#14364,#14365,#14366,#14367,#14368,
#14369,#14370,#14371,#14372,#14373,#14374,#14375,#14376,#14377,#14378,#14379,
#14380,#14381,#14382,#14383,#14384,#14385,#14386,#14387,#14388,#14389,#14390,
#14391,#14392,#14393,#14394,#14395,#14396,#14397,#14398,#14399,#14400,#14401,
#14402,#14403,#14404,#14405,#14406,#14407,#14408,#14409,#14410,#14411,#14412,
#14413,#14414,#14415,#14416,#14417,#14418,#14419,#14420,#14421,#14422,#14423,
#14424,#14425,#14426,#14427,#14428,#14429,#14430,#14431,#14432,#14433,#14434,
#14435,#14436,#14437,#14438,#14439,#14440,#14441,#14442,#14443,#14444,#14445,
#14446,#14447,#14448,#14449,#14450,#14451,#14452,#14453,#14454,#14455,#14456,
#14457,#14458,#14459,#14460,#14461,#14462,#14463,#14464,#14465,#14466,#14467,
#14468,#14469,#14470,#14471,#14472,#14473,#14474,#14475,#14476,#14477,#14478,
#14479,#14480,#14481,#14482,#14483,#14484,#14485,#14486,#14487,#14488,#14489,
#14490,#14491,#14492,#14493,#14494,#14495,#14496,#14497,#14498,#14499,#14500,
#14501,#14502,#14503,#14504,#14505,#14506,#14507,#14508,#14509,#14510,#14511,
#14512,#14513,#14514,#14515,#14516,#14517,#14518,#14519,#14520,#14521,#14522,
#14523,#14524,#14525,#14526,#14527,#14528,#14529,#14530,#14531,#14532,#14533,
#14534,#14535,#14536,#14537,#14538,#14539,#14540,#14541,#14542,#14543,#14544,
#14545,#14546,#14547,#14548,#14549,#14550,#14551,#14552,#14553,#14554,#14555,
#14556,#14557,#14558,#14559,#14560,#14561,#14562,#14563,#14564,#14565,#14566,
#14567,#14568,#14569,#14570,#14571,#14572,#14573,#14574,#14575,#14576,#14577,
#14578,#14579,#14580,#14581,#14582,#14583,#14584,#14585,#14586,#14587,#14588,
#14589,#14590,#14591,#14592,#14593,#14594,#14595,#14596,#14597,#14598,#14599,
#14600,#14601,#14602,#14603,#14604,#14605,#14606,#14607,#14608,#14609,#14610,
#14611),.UNSPECIFIED.,.F.,.F.,(4,2,2,2,2,2,2,2,2,2,2,2,2,2,2,2,2,2,2,2,
2,2,2,2,2,2,2,2,2,2,2,2,2,2,2,2,2,2,2,2,2,2,2,2,2,2,2,2,2,2,2,2,2,2,2,2,
2,2,2,2,2,2,2,2,2,2,2,2,2,2,2,2,2,2,2,2,2,2,2,2,2,2,2,2,2,2,2,2,2,2,2,2,
2,2,2,2,2,2,2,2,2,2,2,2,2,2,2,2,2,2,2,2,2,2,2,2,2,2,2,2,2,2,2,2,2,2,2,2,
2,2,2,2,2,2,2,2,2,2,2,2,2,2,2,2,2,4),(-2.6922410793174,-2.68713462272044,
-2.64823997998648,-2.62408582515161,-2.61450042249326,-2.61312557337638,
-2.61242574270667,-2.61186446364603,-2.61121958928161,-2.61012871639063,
-2.60621286827792,-2.60561728037059,-2.50244536075739,-2.46034444360088,
-2.45376363155032,-2.45240811610361,-2.45116107621633,-2.45017190993429,
-2.44918897635062,-2.44777179075376,-2.44379548677097,-2.44214989183045,
-2.35711071102754,-2.331909315746,-2.29283407919076,-2.29042678077883,-2.28954818758804,
-2.28895675687757,-2.28838339815196,-2.28769259177839,-2.28597024774855,
-2.270277566579,-2.22975440958395,-2.17871775924245,-2.15058635241785,-2.13196261563494,
-2.12945305774455,-2.12818757464308,-2.12727448816167,-2.12630516097562,
-2.12493767291909,-2.12128365515612,-2.06285430825287,-2.03077692330812,
-1.98320272125178,-1.9827691275745,-1.98211228742657,-1.98099312574363,
-1.96881277315717,-1.96722633012536,-1.96648094994786,-1.96591256137913,
-1.96529993928841,-1.96432476689283,-1.96116788120736,-1.90901210828921,
-1.84748766450742,-1.83134000860834,-1.80960283654488,-1.80672794264587,
-1.80540461505629,-1.80438611967032,-1.80329278402458,-1.8015744786572,
-1.79618406098519,-1.76574598111205,-1.72086324532706,-1.68873903751014,
-1.64735824939117,-1.64475232609375,-1.64381391807694,-1.64326982933107,
-1.64271553751978,-1.64199820900581,-1.6412086522539,-1.63990912343395,
-1.6372977843104,-1.60941290023342,-1.49017200065016,-1.48462612211848,
-1.48281988023028,-1.48181838956609,-1.48081242586797,-1.47956903877008,
-1.47716516419016,-1.4616084856093,-1.42567471149632,-1.33270251610063,
-1.32253259850076,-1.3210074890702,-1.32028528398105,-1.31972042577709,
-1.31910934427433,-1.31811887402089,-1.31694145154479,-1.31466018507528,
-1.23135337311723,-1.19359734994182,-1.1637887241948,-1.16097645325252,
-1.15961582414204,-1.15864845161507,-1.15773484750122,-1.15646490249426,
-1.15393294366652,-1.13454213039803,-1.10434983166698,-1.00349420131543,
-1.00105446347532,-0.998426007332181,-0.997484208043545,-0.996939417015215,
-0.996385338786349,-0.995668860798337,-0.994881252118572,-0.993586459037281,
-0.990988183862428,-0.98430248978452,-0.958260620862715,-0.872080674700547,
-0.865052497408185,-0.85978181409044,-0.855181814541239,-0.853109715711091,
-0.849293231856371,-0.845532490556877,-0.838770700936585,-0.836817912953404,
-0.835672171381988,-0.834675141219425,-0.833430981514482,-0.831024353935636,
-0.815408676963877,-0.779259016791593,-0.768382155130384,-0.686574073417267,
-0.676406981929468,-0.674881783655769,-0.674159475809447,-0.673594510143407,
-0.672983285351853,-0.671993516232607,-0.670816451190077,-0.668536307392394,
-0.662936658298539,-0.661877334975925),.UNSPECIFIED.);
#93=B_SPLINE_CURVE_WITH_KNOTS('',3,(#14617,#14618,#14619,#14620,#14621,
#14622,#14623,#14624,#14625,#14626,#14627,#14628,#14629,#14630,#14631,#14632,
#14633,#14634,#14635,#14636,#14637,#14638,#14639,#14640,#14641,#14642,#14643,
#14644,#14645,#14646,#14647,#14648,#14649,#14650,#14651,#14652,#14653,#14654,
#14655,#14656,#14657,#14658,#14659,#14660,#14661,#14662,#14663,#14664,#14665,
#14666,#14667,#14668,#14669,#14670,#14671,#14672,#14673,#14674,#14675,#14676,
#14677,#14678,#14679,#14680,#14681,#14682,#14683,#14684,#14685,#14686,#14687,
#14688,#14689,#14690,#14691,#14692,#14693,#14694,#14695,#14696,#14697,#14698,
#14699,#14700,#14701,#14702,#14703,#14704,#14705,#14706,#14707,#14708,#14709,
#14710,#14711,#14712,#14713,#14714,#14715,#14716,#14717,#14718,#14719,#14720,
#14721,#14722,#14723,#14724,#14725,#14726,#14727,#14728,#14729,#14730,#14731,
#14732,#14733,#14734,#14735,#14736,#14737,#14738,#14739,#14740,#14741,#14742,
#14743,#14744,#14745,#14746,#14747,#14748,#14749,#14750,#14751,#14752,#14753,
#14754,#14755,#14756,#14757,#14758,#14759,#14760,#14761,#14762,#14763,#14764,
#14765,#14766,#14767,#14768,#14769,#14770,#14771,#14772,#14773,#14774,#14775,
#14776,#14777,#14778,#14779,#14780,#14781,#14782,#14783,#14784,#14785,#14786,
#14787,#14788,#14789,#14790,#14791,#14792,#14793,#14794,#14795,#14796,#14797,
#14798,#14799,#14800,#14801,#14802,#14803,#14804,#14805,#14806,#14807,#14808,
#14809,#14810,#14811,#14812,#14813,#14814,#14815,#14816,#14817,#14818,#14819,
#14820,#14821,#14822,#14823,#14824,#14825,#14826,#14827,#14828,#14829,#14830,
#14831,#14832,#14833,#14834,#14835,#14836,#14837,#14838,#14839,#14840,#14841,
#14842,#14843,#14844,#14845,#14846,#14847,#14848,#14849,#14850,#14851,#14852),
 .UNSPECIFIED.,.F.,.F.,(4,2,2,2,2,2,2,2,2,2,2,2,2,2,2,2,2,2,2,2,2,2,2,2,
2,2,2,2,2,2,2,2,2,2,2,2,2,2,2,2,2,2,2,2,2,2,2,2,2,2,2,2,2,2,2,2,2,2,2,2,
2,2,2,2,2,2,2,2,2,2,2,2,2,2,2,2,2,2,2,2,2,2,2,2,2,2,2,2,2,2,2,2,2,2,2,2,
2,2,2,2,2,2,2,2,2,2,2,2,2,2,2,2,2,2,2,2,2,4),(-1.3706021342809,-1.33968790873535,
-1.33401856145952,-1.33219611259199,-1.33119124182556,-1.33020562887945,
-1.32900320820066,-1.32770815951129,-1.32567126229208,-1.32179411806332,
-1.28694575622446,-1.18969573353665,-1.18724711149206,-1.17210366014068,
-1.17056744965157,-1.16981741516319,-1.16928094905498,-1.16876880551868,
-1.16803922229462,-1.16651679777185,-1.15086122351035,-1.13346846105473,
-1.01711551700477,-1.01084781452235,-1.00895174280275,-1.00793206835958,
-1.00702199189956,-1.00587166081457,-1.00386491049888,-1.00142321564038,
-0.996459223325355,-0.983561038025477,-0.953233618460723,-0.860087611558867,
-0.848637054403729,-0.847057996362212,-0.846325398928482,-0.845759001205586,
-0.84514051388519,-0.844139117633422,-0.84074713483859,-0.819288600678181,
-0.804879385123748,-0.79419062765631,-0.706327556382138,-0.704355576413767,
-0.702290172124463,-0.688799318849554,-0.68655653396867,-0.685221665917053,
-0.684201348806267,-0.683134805995026,-0.68149517466419,-0.679587812504406,
-0.676045958981582,-0.667851210282897,-0.643240497144552,-0.555880283953574,
-0.544980834416855,-0.543055155749907,-0.541784414057877,-0.525796932951882,
-0.524066125889073,-0.523373908728048,-0.522800161807121,-0.522209173753513,
-0.521332755836952,-0.518940682511649,-0.480883771885869,-0.470737638773909,
-0.462440339963734,-0.455371834935408,-0.449211566916693,-0.443764109072833,
-0.391834080392399,-0.385723458468287,-0.384350631729943,-0.383139853290937,
-0.381890920660856,-0.380734584892317,-0.378726169769955,-0.378274759633109,
-0.376211384241394,-0.374396806030457,-0.36681284380364,-0.363990923932303,
-0.362627781209224,-0.361659596428653,-0.360686126573825,-0.359412315683539,
-0.356838541751506,-0.353525769315386,-0.346035527004777,-0.323716324096793,
-0.304845271156971,-0.2244268547986,-0.217235472111384,-0.216807594226912,
-0.214523303241535,-0.20262634171097,-0.201029914946419,-0.200293970633825,
-0.199727004845841,-0.199109983184496,-0.198115379408065,-0.194786555305278,
-0.17398250401675,-0.0770206757634432,-0.0714024034177756,-0.0435884196513709,
-0.0405174833187884,-0.0392804771056761,-0.0382511397177548,-0.0373052319327293,
-0.0362747903774904,-0.0348785279011245,-0.0326008214399287,-0.000960744511183088),
 .UNSPECIFIED.);
#94=B_SPLINE_CURVE_WITH_KNOTS('',3,(#14853,#14854,#14855,#14856,#14857,
#14858,#14859,#14860,#14861,#14862,#14863,#14864,#14865,#14866,#14867,#14868,
#14869,#14870,#14871,#14872,#14873,#14874,#14875,#14876,#14877,#14878,#14879,
#14880,#14881,#14882,#14883,#14884,#14885,#14886,#14887,#14888,#14889,#14890,
#14891,#14892,#14893,#14894,#14895,#14896,#14897,#14898,#14899,#14900,#14901,
#14902,#14903,#14904,#14905,#14906,#14907,#14908,#14909,#14910,#14911,#14912,
#14913,#14914,#14915,#14916,#14917,#14918,#14919,#14920,#14921,#14922,#14923,
#14924,#14925,#14926,#14927,#14928,#14929,#14930,#14931,#14932,#14933,#14934,
#14935,#14936,#14937,#14938,#14939,#14940,#14941,#14942,#14943,#14944,#14945,
#14946,#14947,#14948,#14949,#14950,#14951,#14952,#14953,#14954),
 .UNSPECIFIED.,.F.,.F.,(4,2,2,2,2,2,2,2,2,2,2,2,2,2,2,2,2,2,2,2,2,2,2,2,
2,2,2,2,2,2,2,2,2,2,2,2,2,2,2,2,2,2,2,2,2,2,2,2,2,2,4),(-4.06089064309864,
-3.96335235672118,-3.94175675000815,-3.93835198066777,-3.93734921724052,
-3.93673043128563,-3.93616413894775,-3.93543219329238,-3.93385652356892,
-3.92249076690551,-3.91961350040436,-3.91861505179853,-3.91748448977263,
-3.91660111691796,-3.87731498072753,-3.82630983363265,-3.81059068443923,
-3.78986722396061,-3.78279530828148,-3.77806295378722,-3.77643045528318,
-3.77548755109764,-3.7744768041985,-3.77318713787788,-3.77055829171436,
-3.7545630006739,-3.74990497964328,-3.74591858543458,-3.70217391470195,
-3.67084846939447,-3.61859619825551,-3.61540924804387,-3.61443062183609,
-3.61381722569045,-3.61324911756206,-3.61250549498024,-3.61086773933177,
-3.60682639938017,-3.51400656001251,-3.47646817282647,-3.46331420601142,
-3.45827684851337,-3.45580848090533,-3.45378609440468,-3.45263089382435,
-3.45172366915353,-3.45070819523185,-3.44883324870267,-3.44274305947501,
-3.43878172892971,-3.3998905608284),.UNSPECIFIED.);
#95=B_SPLINE_CURVE_WITH_KNOTS('',3,(#14956,#14957,#14958,#14959,#14960,
#14961,#14962,#14963,#14964,#14965,#14966,#14967,#14968,#14969,#14970,#14971,
#14972,#14973,#14974,#14975,#14976,#14977,#14978,#14979,#14980,#14981,#14982,
#14983,#14984,#14985,#14986,#14987,#14988,#14989,#14990,#14991,#14992,#14993,
#14994,#14995,#14996,#14997,#14998,#14999,#15000,#15001,#15002,#15003,#15004,
#15005,#15006,#15007,#15008,#15009,#15010,#15011,#15012,#15013,#15014,#15015,
#15016,#15017,#15018,#15019,#15020,#15021,#15022,#15023,#15024,#15025,#15026,
#15027,#15028,#15029,#15030,#15031,#15032,#15033,#15034,#15035,#15036,#15037,
#15038,#15039,#15040,#15041,#15042,#15043,#15044,#15045,#15046,#15047,#15048,
#15049,#15050,#15051,#15052,#15053,#15054,#15055,#15056,#15057,#15058,#15059,
#15060,#15061),.UNSPECIFIED.,.F.,.F.,(4,2,2,2,2,2,2,2,2,2,2,2,2,2,2,2,2,
2,2,2,2,2,2,2,2,2,2,2,2,2,2,2,2,2,2,2,2,2,2,2,2,2,2,2,2,2,2,2,2,2,2,2,4),
(-0.661877334975925,-0.643648093147668,-0.598629952563144,-0.593209413012196,
-0.519753098729238,-0.515191858152316,-0.513524045209656,-0.512550046423522,
-0.511638474291198,-0.510384341549493,-0.507930040296465,-0.491011222933779,
-0.449850944372571,-0.440733349264975,-0.433186533921284,-0.426761311763646,
-0.421189247754163,-0.416290444791287,-0.371545985948876,-0.370380562012174,
-0.369457716532448,-0.353765601871672,-0.352043229174806,-0.351352398356726,
-0.350779015061414,-0.350252870931183,-0.34944154868183,-0.347455288281762,
-0.344672343238775,-0.33733227221629,-0.312022014438792,-0.224118836026523,
-0.194673419639501,-0.191869549367345,-0.190510912482517,-0.189544015592249,
-0.188630095191333,-0.187358491820614,-0.184818789933339,-0.165163829781162,
-0.134271791019828,-0.0559302248217822,-0.0522241009295653,-0.0465244163130091,
-0.0307401376884319,-0.0290151397822052,-0.0283238822308065,-0.0277503922061148,
-0.0272242268041416,-0.0266439166341936,-0.0258493377915546,-0.0245377297322901,
-0.00096062754245072),.UNSPECIFIED.);
#96=B_SPLINE_CURVE_WITH_KNOTS('',3,(#15062,#15063,#15064,#15065,#15066,
#15067,#15068,#15069,#15070,#15071,#15072,#15073,#15074,#15075,#15076,#15077,
#15078,#15079,#15080,#15081,#15082,#15083,#15084,#15085,#15086,#15087,#15088,
#15089,#15090,#15091,#15092,#15093,#15094,#15095,#15096,#15097,#15098,#15099,
#15100,#15101,#15102,#15103,#15104,#15105,#15106,#15107,#15108,#15109,#15110,
#15111,#15112,#15113,#15114,#15115,#15116,#15117,#15118,#15119,#15120,#15121,
#15122,#15123,#15124,#15125,#15126,#15127,#15128,#15129,#15130,#15131,#15132,
#15133,#15134,#15135,#15136,#15137,#15138,#15139,#15140,#15141,#15142,#15143,
#15144,#15145,#15146,#15147,#15148,#15149,#15150,#15151,#15152,#15153,#15154,
#15155,#15156,#15157,#15158,#15159,#15160,#15161,#15162,#15163,#15164,#15165,
#15166,#15167,#15168,#15169,#15170,#15171,#15172,#15173,#15174,#15175,#15176,
#15177,#15178,#15179,#15180,#15181,#15182,#15183,#15184,#15185,#15186,#15187,
#15188,#15189,#15190,#15191,#15192,#15193,#15194,#15195,#15196,#15197,#15198,
#15199,#15200,#15201,#15202,#15203),.UNSPECIFIED.,.F.,.F.,(4,3,3,3,3,3,
3,3,3,3,3,3,3,3,3,3,3,3,3,3,3,3,3,3,3,3,3,3,3,3,3,3,3,3,3,3,3,3,3,3,3,3,
3,3,3,3,3,4),(103.672557568728,103.764546167889,103.856418305638,103.948199630661,
104.039931731389,104.131640502381,104.223351810979,104.315152260498,104.406995790917,
104.49899760578,104.588677186729,104.681750131005,104.774696970642,104.867545341827,
104.960325846482,105.053071168639,105.14580613374,105.238555552081,105.331404192816,
105.424304633428,105.517360529512,105.588391842202,105.681464786478,105.774411626115,
105.867259997299,105.960040501955,106.052785824111,106.145520789212,106.238270207553,
106.331118848288,106.4240192889,106.517075184984,106.588106497675,106.681179441951,
106.774126281588,106.866974652772,106.959755157428,107.052500479584,107.145235444685,
107.237984863027,107.330833503762,107.423733944374,107.516789840458,107.587821153148,
107.680878189667,107.773824604379,107.866666658252,107.909967710001),
 .UNSPECIFIED.);
#97=B_SPLINE_CURVE_WITH_KNOTS('',3,(#15208,#15209,#15210,#15211,#15212,
#15213,#15214,#15215,#15216,#15217,#15218,#15219,#15220,#15221,#15222,#15223,
#15224,#15225,#15226,#15227,#15228,#15229,#15230,#15231,#15232,#15233,#15234,
#15235,#15236,#15237,#15238,#15239,#15240,#15241,#15242,#15243,#15244,#15245,
#15246,#15247,#15248,#15249,#15250,#15251,#15252,#15253,#15254,#15255,#15256,
#15257,#15258,#15259,#15260,#15261,#15262,#15263,#15264,#15265,#15266,#15267,
#15268,#15269,#15270,#15271,#15272,#15273,#15274,#15275,#15276,#15277,#15278,
#15279,#15280,#15281,#15282,#15283,#15284,#15285,#15286,#15287,#15288,#15289,
#15290,#15291,#15292,#15293,#15294,#15295,#15296,#15297,#15298,#15299,#15300,
#15301,#15302,#15303,#15304,#15305,#15306,#15307,#15308,#15309,#15310,#15311,
#15312,#15313,#15314,#15315,#15316,#15317,#15318,#15319,#15320,#15321,#15322,
#15323,#15324,#15325,#15326,#15327,#15328,#15329,#15330,#15331,#15332,#15333,
#15334,#15335,#15336,#15337,#15338,#15339,#15340,#15341,#15342,#15343,#15344,
#15345,#15346,#15347,#15348,#15349,#15350,#15351,#15352,#15353,#15354,#15355,
#15356,#15357,#15358,#15359,#15360,#15361,#15362,#15363,#15364,#15365,#15366,
#15367,#15368,#15369,#15370,#15371,#15372,#15373,#15374,#15375,#15376,#15377,
#15378,#15379,#15380,#15381,#15382,#15383,#15384,#15385,#15386,#15387,#15388,
#15389,#15390,#15391,#15392,#15393,#15394,#15395,#15396,#15397,#15398,#15399,
#15400,#15401,#15402,#15403,#15404,#15405,#15406,#15407,#15408,#15409,#15410,
#15411,#15412,#15413,#15414,#15415,#15416,#15417,#15418,#15419,#15420,#15421,
#15422,#15423,#15424,#15425,#15426,#15427,#15428,#15429,#15430,#15431,#15432,
#15433,#15434,#15435,#15436,#15437,#15438,#15439,#15440,#15441,#15442,#15443,
#15444,#15445,#15446,#15447,#15448,#15449,#15450,#15451,#15452,#15453,#15454,
#15455,#15456,#15457,#15458,#15459,#15460,#15461,#15462,#15463,#15464,#15465,
#15466,#15467,#15468,#15469,#15470,#15471,#15472,#15473,#15474,#15475,#15476,
#15477,#15478,#15479,#15480,#15481,#15482,#15483,#15484,#15485,#15486,#15487,
#15488,#15489,#15490,#15491,#15492,#15493),.UNSPECIFIED.,.F.,.F.,(4,2,2,
2,2,2,2,2,2,2,2,2,2,2,2,2,2,2,2,2,2,2,2,2,2,2,2,2,2,2,2,2,2,2,2,2,2,2,2,
2,2,2,2,2,2,2,2,2,2,2,2,2,2,2,2,2,2,2,2,2,2,2,2,2,2,2,2,2,2,2,2,2,2,2,2,
2,2,2,2,2,2,2,2,2,2,2,2,2,2,2,2,2,2,2,2,2,2,2,2,2,2,2,2,2,2,2,2,2,2,2,2,
2,2,2,2,2,2,2,2,2,2,2,2,2,2,2,2,2,2,2,2,2,2,2,2,2,2,2,2,2,2,2,4),(-3.40187331252921,
-3.36412124741289,-3.30968310554371,-3.28608354083431,-3.27410832604247,
-3.27186664126087,-3.27065758594873,-3.2696628274175,-3.26864346275063,
-3.26674888429633,-3.26049364152775,-3.15332102102897,-3.1257659449776,
-3.11580735230516,-3.11232706015273,-3.11072202079272,-3.10980744504818,
-3.10917884723728,-3.1085758553691,-3.10802293458334,-3.10729205971141,
-3.10572208952273,-3.09449893029603,-3.09219247862971,-3.08920596146183,
-3.08809569036755,-3.07839057879091,-2.98858825442644,-2.96381425827186,
-2.95100065462571,-2.94871591170645,-2.94749755404456,-2.94649287895053,
-2.94547659206097,-2.94359760397715,-2.93747391092113,-2.82773537074217,
-2.78880149043531,-2.78733927968874,-2.78648263518727,-2.78571664844179,
-2.78515451385923,-2.78462497140541,-2.78390128039199,-2.78209775218967,
-2.76173234952193,-2.75726073354586,-2.69909324078275,-2.66508296371755,
-2.64039610954141,-2.62783194945586,-2.62555925016183,-2.62434330631159,
-2.62343608172097,-2.62229961111581,-2.62038884459864,-2.61399876941403,
-2.610051734052,-2.60824352892161,-2.60733015666557,-2.60621263482647,-2.6041198166312,
-2.60224541782368,-2.60101789112454,-2.59932561643077,-2.59308879565364,
-2.50205677295237,-2.48155234346152,-2.46650122405959,-2.46467469179825,
-2.46367188647583,-2.46300648749872,-2.46237763301092,-2.46182905485978,
-2.46113103489759,-2.46005629618995,-2.45522619501713,-2.36265078853053,
-2.3402540630495,-2.31659704727469,-2.30459564179387,-2.30235197212246,
-2.30114222195348,-2.30014708758433,-2.29912750990517,-2.29723304092275,
-2.29098231587382,-2.18671154325818,-2.15674679769867,-2.14641390693721,
-2.14097511127026,-2.13979909461423,-2.13914157569107,-2.13863723003993,
-2.13806439216471,-2.1369837437247,-2.13328004243408,-2.13238636149393,
-2.12981840417762,-2.12824965721844,-2.12691426838688,-2.03243562210988,
-2.01027382174837,-1.98259601532943,-1.9795283221164,-1.97829166807945,
-1.97726224509052,-1.97620817401335,-1.97467215817602,-1.9706342356214,
-1.91585480950935,-1.85558843051331,-1.84039005226584,-1.83240927518667,
-1.81860824190332,-1.81710973959543,-1.816368997954,-1.81583494124016,-1.81526424800612,
-1.81449242717506,-1.81274657021488,-1.7717242492526,-1.66353824274835,
-1.6574001086916,-1.65551917891161,-1.65450238888879,-1.65353048984947,
-1.65235227216252,-1.65109083620079,-1.64913385871923,-1.64546457146241,
-1.61367682834028,-1.56791778459778,-1.4984820109138,-1.49448297144557,
-1.49338328522574,-1.49273631606901,-1.49217519101371,-1.49147808848675,
-1.49011658876561,-1.48091265233273,-1.45831578482449,-1.3706021342809),
 .UNSPECIFIED.);
#98=B_SPLINE_CURVE_WITH_KNOTS('',3,(#15495,#15496,#15497,#15498,#15499,
#15500,#15501,#15502,#15503,#15504,#15505,#15506,#15507,#15508,#15509,#15510,
#15511,#15512,#15513,#15514,#15515,#15516,#15517,#15518,#15519,#15520,#15521,
#15522,#15523,#15524,#15525,#15526,#15527,#15528,#15529,#15530,#15531,#15532,
#15533,#15534,#15535,#15536,#15537,#15538,#15539,#15540,#15541,#15542,#15543,
#15544,#15545,#15546,#15547,#15548,#15549,#15550,#15551,#15552,#15553,#15554,
#15555,#15556,#15557,#15558,#15559,#15560,#15561,#15562,#15563,#15564),
 .UNSPECIFIED.,.F.,.F.,(4,3,3,3,3,3,3,3,3,3,3,3,3,3,3,3,3,3,3,3,3,3,3,4),
(107.909967710001,108.002728714755,108.095466118645,108.188204737573,108.280969381588,
108.373839389017,108.466771599224,108.559846662765,108.587535808621,108.680608752897,
108.773555592534,108.866403963719,108.959184468374,109.051929790531,109.144664755632,
109.237414173973,109.330262814708,109.42316325532,109.516219151404,109.587250464094,
109.693194910979,109.798742509158,109.903582591639,109.955742875448),
 .UNSPECIFIED.);
#99=B_SPLINE_CURVE_WITH_KNOTS('',3,(#15565,#15566,#15567,#15568,#15569,
#15570,#15571,#15572,#15573,#15574,#15575,#15576,#15577,#15578,#15579,#15580,
#15581,#15582,#15583,#15584,#15585,#15586,#15587,#15588,#15589,#15590,#15591,
#15592,#15593,#15594,#15595,#15596,#15597,#15598,#15599,#15600,#15601,#15602,
#15603,#15604,#15605,#15606,#15607,#15608,#15609,#15610,#15611,#15612,#15613,
#15614,#15615,#15616,#15617,#15618,#15619,#15620,#15621,#15622,#15623,#15624,
#15625,#15626,#15627,#15628,#15629,#15630,#15631,#15632,#15633,#15634,#15635,
#15636,#15637,#15638,#15639,#15640,#15641,#15642,#15643,#15644,#15645,#15646,
#15647,#15648,#15649,#15650,#15651,#15652,#15653,#15654,#15655,#15656,#15657,
#15658,#15659,#15660,#15661,#15662,#15663,#15664,#15665,#15666,#15667,#15668,
#15669,#15670,#15671,#15672,#15673,#15674,#15675,#15676,#15677,#15678,#15679,
#15680,#15681,#15682,#15683,#15684,#15685,#15686,#15687,#15688,#15689,#15690,
#15691,#15692,#15693,#15694,#15695,#15696,#15697,#15698,#15699,#15700,#15701,
#15702,#15703,#15704,#15705,#15706,#15707,#15708,#15709,#15710,#15711,#15712,
#15713,#15714,#15715,#15716,#15717,#15718,#15719,#15720,#15721,#15722,#15723,
#15724,#15725,#15726,#15727,#15728,#15729,#15730,#15731,#15732,#15733,#15734,
#15735,#15736,#15737,#15738,#15739,#15740,#15741,#15742,#15743,#15744,#15745,
#15746,#15747,#15748,#15749,#15750,#15751,#15752,#15753,#15754,#15755,#15756,
#15757,#15758,#15759,#15760,#15761,#15762,#15763,#15764,#15765,#15766,#15767,
#15768,#15769,#15770,#15771,#15772,#15773,#15774,#15775,#15776,#15777,#15778,
#15779,#15780,#15781,#15782,#15783,#15784,#15785,#15786,#15787,#15788,#15789,
#15790,#15791,#15792,#15793,#15794),.UNSPECIFIED.,.F.,.F.,(4,2,2,2,2,2,
2,2,2,2,2,2,2,2,2,2,2,2,2,2,2,2,2,2,2,2,2,2,2,2,2,2,2,2,2,2,2,2,2,2,2,2,
2,2,2,2,2,2,2,2,2,2,2,2,2,2,2,2,2,2,2,2,2,2,2,2,2,2,2,2,2,2,2,2,2,2,2,2,
2,2,2,2,2,2,2,2,2,2,2,2,2,2,2,2,2,2,2,2,2,2,2,2,2,2,2,2,2,2,2,2,2,2,2,2,
4),(-4.06398272956981,-4.02654081354827,-4.02446721588437,-4.02315633577637,
-4.02215694944922,-4.0211965879973,-4.02024817632782,-4.01896165171567,
-4.01644672542685,-3.99681327641816,-3.99055248907445,-3.98295092746506,
-3.97726740099106,-3.89472643356396,-3.86560891437986,-3.86293525861883,
-3.86099843345383,-3.86019292754274,-3.85961598417565,-3.85908953963678,
-3.85837891222914,-3.85699968832063,-3.84670078631966,-3.75261826487865,
-3.7278174683751,-3.71096634124997,-3.70490944193815,-3.70072162314768,
-3.69916617934145,-3.69822406961208,-3.69720511181753,-3.69588259377633,
-3.69301503694688,-3.68507315740922,-3.68273549462731,-3.68149055527552,
-3.68044338737323,-3.67978478709712,-3.6757927034971,-3.67459643863632,
-3.67310037544265,-3.66849699075183,-3.6611111438708,-3.60923402252179,
-3.60341269043478,-3.57432184551967,-3.54879406223136,-3.53887235319483,
-3.53748554181394,-3.53678297630624,-3.53627455231809,-3.53572725505765,
-3.53477405051823,-3.53207146328394,-3.52971850461946,-3.44456140600255,
-3.40691101698071,-3.38849483783438,-3.38202346311345,-3.37905135526909,
-3.37669424445445,-3.37546602027281,-3.37447386328896,-3.37333523506362,
-3.37141643028461,-3.36496208804944,-3.36104167655824,-3.35926349675722,
-3.35711468686016,-3.35503022912267,-3.35015563032939,-3.34515601621909,
-3.26083015931368,-3.24957928187052,-3.21629008336503,-3.21445309556672,
-3.21366482647362,-3.21309108577417,-3.21256088286679,-3.21183543072234,
-3.21039825905946,-3.19852592481607,-3.13956530349988,-3.09330829475832,
-3.0685063857932,-3.06010413968315,-3.05649486624137,-3.05373321458639,
-3.05242208983903,-3.05145815311605,-3.05050426580544,-3.04919648771829,
-3.04590838953056,-3.00566473059495,-2.96728200593774,-2.92047610553774,
-2.90090444746831,-2.89238870437015,-2.89105279108915,-2.89036078957903,
-2.88979970071162,-2.88923318120779,-2.8881845453131,-2.88475769855497,
-2.82866084758995,-2.73688129554516,-2.7332534662231,-2.73131225924506,
-2.72964797470032,-2.72857582118082,-2.72755680439306,-2.72623343293228,
-2.72336095381366,-2.70172361874953,-2.69388977725967),.UNSPECIFIED.);
#100=B_SPLINE_CURVE_WITH_KNOTS('',3,(#15800,#15801,#15802,#15803,#15804,
#15805,#15806,#15807,#15808,#15809,#15810,#15811,#15812,#15813,#15814,#15815,
#15816,#15817,#15818,#15819,#15820,#15821,#15822,#15823,#15824,#15825,#15826,
#15827,#15828,#15829,#15830,#15831,#15832,#15833,#15834,#15835,#15836,#15837,
#15838,#15839,#15840,#15841,#15842,#15843,#15844,#15845,#15846,#15847,#15848,
#15849,#15850,#15851,#15852,#15853,#15854,#15855,#15856,#15857,#15858,#15859,
#15860,#15861,#15862,#15863,#15864,#15865,#15866,#15867,#15868,#15869,#15870,
#15871,#15872,#15873,#15874,#15875,#15876,#15877,#15878,#15879,#15880,#15881,
#15882,#15883,#15884,#15885,#15886,#15887,#15888,#15889,#15890,#15891,#15892,
#15893,#15894,#15895,#15896,#15897,#15898,#15899,#15900,#15901,#15902,#15903,
#15904,#15905,#15906,#15907,#15908,#15909,#15910,#15911,#15912,#15913,#15914,
#15915,#15916,#15917,#15918,#15919,#15920,#15921,#15922,#15923,#15924,#15925,
#15926,#15927,#15928,#15929,#15930,#15931,#15932,#15933,#15934,#15935,#15936,
#15937,#15938,#15939,#15940,#15941,#15942,#15943,#15944,#15945,#15946,#15947,
#15948,#15949,#15950,#15951,#15952,#15953,#15954,#15955,#15956,#15957,#15958,
#15959,#15960,#15961,#15962,#15963,#15964,#15965,#15966,#15967,#15968,#15969,
#15970,#15971,#15972,#15973,#15974,#15975,#15976,#15977,#15978,#15979,#15980,
#15981,#15982,#15983,#15984,#15985,#15986,#15987,#15988,#15989,#15990,#15991,
#15992,#15993,#15994,#15995,#15996,#15997,#15998,#15999,#16000,#16001,#16002,
#16003,#16004,#16005,#16006,#16007,#16008,#16009,#16010,#16011,#16012,#16013,
#16014,#16015,#16016,#16017,#16018,#16019,#16020,#16021,#16022,#16023,#16024,
#16025),.UNSPECIFIED.,.F.,.F.,(4,2,2,2,2,2,2,2,2,2,2,2,2,2,2,2,2,2,2,2,
2,2,2,2,2,2,2,2,2,2,2,2,2,2,2,2,2,2,2,2,2,2,2,2,2,2,2,2,2,2,2,2,2,2,2,2,
2,2,2,2,2,2,2,2,2,2,2,2,2,2,2,2,2,2,2,2,2,2,2,2,2,2,2,2,2,2,2,2,2,2,2,2,
2,2,2,2,2,2,2,2,2,2,2,2,2,2,2,2,2,2,2,2,4),(-1.37047652883368,-1.32015777460888,
-1.31866669325793,-1.31713841650632,-1.31469840959735,-1.31341532264545,
-1.30992192873267,-1.30886572146225,-1.30829787964147,-1.30774832096595,
-1.30707857700824,-1.30635572846671,-1.30521599870066,-1.30303483706847,
-1.28262796328326,-1.26941444163345,-1.18240240930743,-1.15193855433878,
-1.14911052091622,-1.14774587239272,-1.14677727201455,-1.1458638296299,
-1.14459620530877,-1.14207645991256,-1.12311889143595,-1.0940855982088,
-0.991401973109268,-0.990372138340198,-0.986748198684808,-0.98567666999011,
-0.98510568741204,-0.984556342112059,-0.983888687264163,-0.983171268684019,
-0.982044564542278,-0.979897811491443,-0.974737869163734,-0.959430256075991,
-0.946215905879761,-0.859252288528087,-0.828716109103562,-0.825886092919283,
-0.824520857644493,-0.8235520078953,-0.822638465682966,-0.821370917252886,
-0.818852097037579,-0.799935527825703,-0.771015318814669,-0.758535945108684,
-0.747263999051615,-0.668316289869753,-0.667256980918422,-0.663622509221959,
-0.662549773116947,-0.661978548022892,-0.661429132480898,-0.660764599594385,
-0.660048822273431,-0.658926026716913,-0.656789537254835,-0.651662985562846,
-0.636072203056154,-0.614635644907025,-0.50957791636679,-0.503424390670518,
-0.501541571629006,-0.50052437820154,-0.499519535850313,-0.498302022789894,
-0.496021957196585,-0.483310172221965,-0.458504351789894,-0.430070672743369,
-0.421427016637148,-0.414111829165556,-0.407776380358645,-0.390596515324826,
-0.361798197447345,-0.341726506647209,-0.339929551797598,-0.339207013956112,
-0.338677782721056,-0.338115520135312,-0.337349416180117,-0.336491757610056,
-0.335027054029267,-0.331953504174857,-0.32355009940443,-0.301903294756425,
-0.186219288193886,-0.180223076974626,-0.178359645701891,-0.177346535773835,
-0.176341692319634,-0.175118351602603,-0.172810012876453,-0.159503064781469,
-0.144312393986993,-0.113889603883803,-0.0311711628329554,-0.0277257105112761,
-0.0255750214978552,-0.0239273561288705,-0.0176862322117764,-0.0165103725667851,
-0.0157813568243212,-0.0152362952012227,-0.0147109123534575,-0.0141006338598269,
-0.0132307052039227,-0.011735848888498,-0.000960909134095826),
 .UNSPECIFIED.);
#101=B_SPLINE_CURVE_WITH_KNOTS('',3,(#16026,#16027,#16028,#16029,#16030,
#16031,#16032,#16033,#16034,#16035,#16036,#16037,#16038,#16039,#16040,#16041,
#16042,#16043,#16044,#16045,#16046,#16047,#16048,#16049,#16050,#16051,#16052,
#16053,#16054,#16055,#16056,#16057,#16058,#16059,#16060,#16061,#16062,#16063,
#16064,#16065,#16066,#16067,#16068,#16069,#16070,#16071,#16072,#16073,#16074,
#16075,#16076,#16077,#16078,#16079,#16080,#16081,#16082,#16083,#16084,#16085,
#16086,#16087,#16088,#16089,#16090,#16091,#16092,#16093,#16094,#16095,#16096,
#16097,#16098,#16099,#16100,#16101,#16102,#16103,#16104,#16105,#16106,#16107,
#16108,#16109,#16110,#16111,#16112,#16113,#16114,#16115,#16116,#16117,#16118,
#16119,#16120,#16121,#16122,#16123,#16124,#16125,#16126,#16127,#16128,#16129,
#16130,#16131,#16132,#16133,#16134,#16135),.UNSPECIFIED.,.F.,.F.,(4,2,2,
2,2,2,2,2,2,2,2,2,2,2,2,2,2,2,2,2,2,2,2,2,2,2,2,2,2,2,2,2,2,2,2,2,2,2,2,
2,2,2,2,2,2,2,2,2,2,2,2,2,2,2,4),(-4.06305007721485,-3.97924169820498,-3.9244464609644,
-3.9190345797772,-3.91731422313055,-3.9162207785557,-3.91520301699057,-3.91388182695187,
-3.91101626260136,-3.90308596809809,-3.90123825875958,-3.8991811117024,
-3.89863748447152,-3.8978367324572,-3.89576500712487,-3.89418233327144,
-3.89297875150491,-3.89166879807271,-3.88550812741958,-3.79491451298384,
-3.76868497009556,-3.76086909432057,-3.75795521282537,-3.75654704327038,
-3.7557126879182,-3.75496272130919,-3.75440362541422,-3.75387023445072,
-3.75313115750644,-3.75163834424098,-3.73800291105518,-3.70971297963672,
-3.68536572454858,-3.6325979423156,-3.60908025085917,-3.59714155810716,
-3.59490212374948,-3.59369368950823,-3.59269913265779,-3.59167970264798,
-3.58978420336728,-3.58351933365664,-3.4764260459048,-3.45722877594643,
-3.44155274378925,-3.43644594432405,-3.43431586889472,-3.43319567853982,
-3.43224424692824,-3.43164226031687,-3.43108906362718,-3.43035608281952,
-3.42877459387615,-3.41725489965834,-3.40187331252921),.UNSPECIFIED.);
#102=B_SPLINE_CURVE_WITH_KNOTS('',3,(#16136,#16137,#16138,#16139,#16140,
#16141,#16142,#16143,#16144,#16145,#16146,#16147,#16148,#16149,#16150,#16151,
#16152,#16153,#16154,#16155,#16156,#16157,#16158,#16159,#16160,#16161,#16162,
#16163,#16164,#16165,#16166,#16167,#16168,#16169,#16170,#16171,#16172,#16173,
#16174,#16175,#16176,#16177,#16178,#16179,#16180,#16181,#16182,#16183,#16184,
#16185,#16186,#16187,#16188,#16189,#16190,#16191,#16192,#16193,#16194,#16195,
#16196,#16197,#16198,#16199,#16200,#16201,#16202,#16203,#16204,#16205,#16206,
#16207,#16208,#16209,#16210,#16211,#16212,#16213,#16214,#16215,#16216,#16217,
#16218,#16219,#16220,#16221,#16222,#16223,#16224,#16225,#16226,#16227,#16228,
#16229,#16230,#16231,#16232,#16233,#16234,#16235,#16236,#16237,#16238,#16239,
#16240,#16241,#16242,#16243,#16244,#16245,#16246,#16247,#16248,#16249,#16250,
#16251,#16252,#16253,#16254,#16255,#16256,#16257,#16258,#16259,#16260,#16261,
#16262,#16263,#16264,#16265,#16266,#16267,#16268,#16269,#16270,#16271,#16272,
#16273,#16274,#16275,#16276,#16277,#16278,#16279,#16280,#16281,#16282,#16283,
#16284,#16285,#16286,#16287,#16288,#16289,#16290,#16291,#16292,#16293,#16294,
#16295,#16296,#16297,#16298,#16299,#16300,#16301,#16302,#16303,#16304,#16305,
#16306,#16307,#16308,#16309,#16310,#16311,#16312,#16313,#16314,#16315,#16316,
#16317,#16318,#16319,#16320,#16321,#16322,#16323,#16324,#16325,#16326,#16327,
#16328,#16329,#16330,#16331,#16332,#16333,#16334,#16335,#16336,#16337,#16338,
#16339,#16340,#16341,#16342,#16343,#16344,#16345,#16346,#16347,#16348,#16349,
#16350,#16351,#16352,#16353,#16354,#16355,#16356,#16357,#16358,#16359,#16360,
#16361,#16362,#16363,#16364,#16365,#16366,#16367,#16368,#16369,#16370,#16371,
#16372,#16373,#16374,#16375,#16376,#16377,#16378,#16379,#16380,#16381,#16382,
#16383,#16384,#16385,#16386,#16387,#16388,#16389,#16390,#16391,#16392,#16393,
#16394,#16395,#16396,#16397,#16398,#16399,#16400,#16401,#16402,#16403,#16404,
#16405,#16406,#16407,#16408,#16409,#16410,#16411,#16412,#16413,#16414,#16415,
#16416,#16417,#16418,#16419,#16420,#16421,#16422,#16423,#16424,#16425),
 .UNSPECIFIED.,.F.,.F.,(4,2,2,2,2,2,2,2,2,2,2,2,2,2,2,2,2,2,2,2,2,2,2,2,
2,2,2,2,2,2,2,2,2,2,2,2,2,2,2,2,2,2,2,2,2,2,2,2,2,2,2,2,2,2,2,2,2,2,2,2,
2,2,2,2,2,2,2,2,2,2,2,2,2,2,2,2,2,2,2,2,2,2,2,2,2,2,2,2,2,2,2,2,2,2,2,2,
2,2,2,2,2,2,2,2,2,2,2,2,2,2,2,2,2,2,2,2,2,2,2,2,2,2,2,2,2,2,2,2,2,2,2,2,
2,2,2,2,2,2,2,2,2,2,2,2,4),(-2.69388977725967,-2.6851136547513,-2.61508267689467,
-2.57346186320606,-2.56874085581754,-2.56761681423595,-2.56697064634882,
-2.5664091192115,-2.56571010875245,-2.56463265998276,-2.55977238602004,
-2.46532306061889,-2.41568959032365,-2.41096053871554,-2.40860405341503,
-2.40717463869383,-2.40587521721452,-2.4048776062012,-2.4039141931778,-2.40256993632514,
-2.39982602501282,-2.39212326781216,-2.3903017890458,-2.38823990838823,
-2.38787532026275,-2.38692370568897,-2.38485288537864,-2.38323576033008,
-2.3820313730094,-2.3807166856708,-2.3751448680323,-2.35820669967274,-2.32027375313843,
-2.28706216750734,-2.24654485926836,-2.24479322940269,-2.24402024177927,
-2.24344923450465,-2.24291529478182,-2.24217533675948,-2.24068036653065,
-2.22700823551189,-2.22590929780619,-2.22031929864552,-2.12518392886676,
-2.09085500383044,-2.08504169249523,-2.08327375147513,-2.0821690422674,
-2.08115373943468,-2.07985371792872,-2.07710294276368,-2.05849088157125,
-2.05698223736249,-2.05042651663368,-2.03207056949148,-1.98163952081821,
-1.92564681838314,-1.92221191363842,-1.92116248378489,-1.92059590049224,
-1.92003498584034,-1.91934354497545,-1.91800977156754,-1.90954056255925,
-1.89021498696306,-1.84481093873609,-1.81454832599172,-1.79436341789003,
-1.76429220620313,-1.76147239776307,-1.76010948432152,-1.75914110446856,
-1.75822704975483,-1.75695727380209,-1.75442853761386,-1.73519315324488,
-1.70542779608413,-1.61955303866336,-1.61750300535891,-1.61730236241659,
-1.61457685229036,-1.61418079831197,-1.61206074665341,-1.60003086215566,
-1.59842886360977,-1.59769167048632,-1.59713759557758,-1.59653690345812,
-1.59591182193447,-1.59500613068263,-1.59342352533907,-1.53777337459545,
-1.44446072373319,-1.43882355023647,-1.43700460201491,-1.43600005926753,
-1.43499362553581,-1.43375350669716,-1.43136795542398,-1.41631078014225,
-1.38228818157669,-1.30454420496675,-1.2773032585065,-1.2753717200684,-1.27462607521874,
-1.27409062056098,-1.27353195134802,-1.2727867131723,-1.27195915095113,
-1.27056808868535,-1.23902434373396,-1.12128239433162,-1.11547286980214,
-1.11363210807778,-1.11262327901102,-1.11171811271651,-1.11052958564131,
-1.10838423209916,-1.09808135107253,-1.07861922967001,-1.01936677984926,
-0.963502042356076,-0.953313039447118,-0.951786579945251,-0.95106391431444,
-0.950515700316939,-0.949909496111643,-0.948941007298574,-0.947795579378007,
-0.945599540308642,-0.940278503737567,-0.929807066247697,-0.906269457025552,
-0.798485071534662,-0.792332489804904,-0.790449756938305,-0.789432565622241,
-0.788427697491999,-0.787210113173972,-0.784929795867358,-0.772213717519427,
-0.747406024807181,-0.69539673935075,-0.662451535145792),.UNSPECIFIED.);
#103=B_SPLINE_CURVE_WITH_KNOTS('',3,(#16430,#16431,#16432,#16433,#16434,
#16435,#16436,#16437,#16438,#16439,#16440,#16441,#16442,#16443,#16444,#16445,
#16446,#16447,#16448,#16449,#16450,#16451,#16452,#16453,#16454,#16455,#16456,
#16457,#16458,#16459,#16460,#16461,#16462,#16463,#16464,#16465,#16466,#16467,
#16468,#16469,#16470,#16471,#16472,#16473,#16474,#16475,#16476,#16477,#16478,
#16479,#16480,#16481,#16482,#16483,#16484,#16485,#16486,#16487,#16488,#16489,
#16490,#16491,#16492,#16493,#16494,#16495,#16496,#16497,#16498,#16499,#16500,
#16501,#16502,#16503,#16504,#16505,#16506,#16507,#16508,#16509,#16510,#16511,
#16512,#16513,#16514,#16515,#16516,#16517,#16518,#16519,#16520,#16521,#16522,
#16523,#16524,#16525,#16526,#16527,#16528,#16529,#16530,#16531,#16532,#16533,
#16534,#16535,#16536,#16537,#16538,#16539,#16540,#16541,#16542,#16543,#16544,
#16545,#16546,#16547,#16548,#16549,#16550,#16551,#16552,#16553,#16554,#16555,
#16556,#16557,#16558,#16559,#16560,#16561,#16562,#16563,#16564,#16565,#16566,
#16567,#16568,#16569,#16570,#16571,#16572,#16573,#16574,#16575,#16576,#16577,
#16578,#16579,#16580,#16581,#16582,#16583,#16584,#16585,#16586,#16587,#16588,
#16589,#16590,#16591,#16592,#16593,#16594,#16595,#16596,#16597,#16598,#16599,
#16600,#16601,#16602,#16603,#16604,#16605,#16606,#16607,#16608,#16609,#16610,
#16611,#16612,#16613,#16614,#16615,#16616,#16617,#16618,#16619,#16620,#16621,
#16622,#16623,#16624,#16625,#16626,#16627,#16628,#16629,#16630,#16631,#16632,
#16633,#16634,#16635,#16636,#16637,#16638,#16639,#16640,#16641,#16642,#16643,
#16644,#16645,#16646,#16647,#16648,#16649,#16650,#16651,#16652,#16653,#16654,
#16655,#16656,#16657,#16658,#16659,#16660,#16661,#16662,#16663,#16664,#16665,
#16666,#16667,#16668,#16669,#16670,#16671,#16672,#16673,#16674,#16675,#16676,
#16677,#16678,#16679,#16680,#16681,#16682,#16683,#16684,#16685,#16686,#16687,
#16688,#16689,#16690,#16691,#16692,#16693,#16694,#16695,#16696,#16697,#16698,
#16699,#16700,#16701,#16702,#16703,#16704,#16705,#16706,#16707,#16708,#16709,
#16710,#16711,#16712,#16713,#16714,#16715,#16716,#16717,#16718,#16719,#16720,
#16721,#16722,#16723),.UNSPECIFIED.,.F.,.F.,(4,2,2,2,2,2,2,2,2,2,2,2,2,
2,2,2,2,2,2,2,2,2,2,2,2,2,2,2,2,2,2,2,2,2,2,2,2,2,2,2,2,2,2,2,2,2,2,2,2,
2,2,2,2,2,2,2,2,2,2,2,2,2,2,2,2,2,2,2,2,2,2,2,2,2,2,2,2,2,2,2,2,2,2,2,2,
2,2,2,2,2,2,2,2,2,2,2,2,2,2,2,2,2,2,2,2,2,2,2,2,2,2,2,2,2,2,2,2,2,2,2,2,
2,2,2,2,2,2,2,2,2,2,2,2,2,2,2,2,2,2,2,2,2,2,2,2,2,4),(-3.40092133460055,
-3.37208765681694,-3.31259585721469,-3.30287183130673,-3.29158746134574,
-3.27527702434948,-3.25717197177797,-3.24888597237038,-3.24756043838951,
-3.24687104916474,-3.24631065909886,-3.24574362833148,-3.24469060006688,
-3.24122141334538,-3.18492861723304,-3.13471292523924,-3.10367567637488,
-3.09425915413262,-3.09033129069727,-3.08827509555633,-3.0869720042922,
-3.08576406007583,-3.08477821218417,-3.08377702567792,-3.08197218007508,
-3.0764366481723,-2.95691450953366,-2.94778867218672,-2.93384219629616,
-2.92575638141298,-2.92443895184821,-2.92375114518264,-2.92319068109186,
-2.92262240457085,-2.92156372400094,-2.91804841430752,-2.86060572053334,
-2.8107650970263,-2.77153003703433,-2.76736954974624,-2.76522490347797,
-2.76388445465652,-2.76264834371954,-2.76165979248964,-2.76067170750641,
-2.75923613124485,-2.75513646594884,-2.69248720588548,-2.60767496413981,
-2.60244469714682,-2.6012832540454,-2.60062903860656,-2.60012490403089,
-2.59954981358211,-2.59845751905003,-2.59464788579388,-2.5939069826619,
-2.49102007879781,-2.44866434201676,-2.44431637222793,-2.44210133799806,
-2.44073133572249,-2.43947506033328,-2.4384839714167,-2.43750558492391,
-2.4358154068616,-2.43110474638592,-2.35765706617824,-2.3317830747326,-2.30270885500215,
-2.28703564616352,-2.27953421961183,-2.27824284099499,-2.2775605428162,
-2.27700558081775,-2.27643540003602,-2.27536728549531,-2.27177116387227,
-2.27064391621703,-2.26817708014668,-2.26662127526971,-2.2652965151977,
-2.23423738136989,-2.17262510943809,-2.1358806488201,-2.12010503638469,
-2.11769231035247,-2.11644687972784,-2.1155364849899,-2.11455884679202,
-2.11316092862699,-2.10931221871045,-2.10778326254082,-2.03148842072216,
-1.96051602255745,-1.95624819748195,-1.95512130961897,-1.95446803346771,
-1.95390746014414,-1.9532186341145,-1.95189657368913,-1.94370358202902,
-1.92667926578758,-1.90207254210137,-1.82788091212383,-1.79813946047098,
-1.79532832375655,-1.79396783153678,-1.79300036966583,-1.79208652947597,
-1.79081601510622,-1.78828204470306,-1.76883578310293,-1.73850093792796,
-1.64532967358157,-1.63388389161355,-1.63230479047895,-1.63157209534144,
-1.6310186656775,-1.63050976754623,-1.62963997049116,-1.62863680051688,
-1.62680932053924,-1.61174540830877,-1.59121009070122,-1.50019332639202,
-1.49399410575801,-1.49262009457137,-1.49141530177704,-1.48988426238721,
-1.48780582812421,-1.487143904756,-1.48612181119718,-1.48477891199037,-1.48394343719247,
-1.48288896541455,-1.47796765379112,-1.47271119125132,-1.47094319661123,
-1.46994915323991,-1.46904227540172,-1.46782966682866,-1.46557240374456,
-1.45330935913335,-1.42909842763686,-1.3874405607434,-1.37047652883368),
 .UNSPECIFIED.);
#104=B_SPLINE_CURVE_WITH_KNOTS('',3,(#16725,#16726,#16727,#16728,#16729,
#16730,#16731,#16732,#16733,#16734,#16735,#16736,#16737,#16738,#16739,#16740,
#16741,#16742,#16743,#16744,#16745,#16746,#16747,#16748,#16749,#16750,#16751,
#16752,#16753,#16754,#16755,#16756,#16757,#16758,#16759,#16760,#16761,#16762,
#16763,#16764,#16765,#16766,#16767,#16768,#16769,#16770,#16771,#16772,#16773,
#16774,#16775,#16776,#16777,#16778,#16779,#16780,#16781,#16782,#16783,#16784,
#16785,#16786,#16787,#16788,#16789,#16790,#16791,#16792,#16793,#16794,#16795,
#16796,#16797,#16798,#16799,#16800,#16801,#16802,#16803,#16804,#16805,#16806,
#16807,#16808,#16809,#16810,#16811,#16812,#16813,#16814,#16815,#16816,#16817,
#16818,#16819,#16820,#16821,#16822,#16823,#16824,#16825,#16826),
 .UNSPECIFIED.,.F.,.F.,(4,2,2,2,2,2,2,2,2,2,2,2,2,2,2,2,2,2,2,2,2,2,2,2,
2,2,2,2,2,2,2,2,2,2,2,2,2,2,2,2,2,2,2,2,2,2,2,2,2,2,4),(-0.662451535145792,
-0.645810712341655,-0.644992134691527,-0.643181364863394,-0.642810009039171,
-0.641843904234085,-0.630229765060319,-0.628802146326098,-0.628079329335985,
-0.627550000758681,-0.626987636164697,-0.626220616775371,-0.625362573165249,
-0.623896974244966,-0.620820950420398,-0.612408530545876,-0.591397558806022,
-0.475122203490112,-0.469095202339053,-0.467227927771129,-0.466213998841606,
-0.465209145512529,-0.46398695277449,-0.461684246652782,-0.448499038718396,
-0.426312219124871,-0.374675550308374,-0.351107634455943,-0.308106662573644,
-0.305833170026884,-0.305035194368541,-0.304485632399452,-0.303937410649659,
-0.303235080666701,-0.301924337612005,-0.30020772363746,-0.296395477252509,
-0.285118325946625,-0.265002978359321,-0.174999601100703,-0.167332949980977,
-0.165301147192011,-0.147579253528041,-0.144868849869099,-0.143563104117543,
-0.142550501601466,-0.14143893040224,-0.139638392106187,-0.133522190226728,
-0.0962401497852022,-0.000962418729335946),.UNSPECIFIED.);
#105=B_SPLINE_CURVE_WITH_KNOTS('',3,(#16827,#16828,#16829,#16830,#16831,
#16832,#16833,#16834,#16835,#16836,#16837,#16838,#16839,#16840,#16841,#16842,
#16843,#16844,#16845,#16846,#16847,#16848,#16849,#16850,#16851,#16852,#16853,
#16854,#16855,#16856,#16857,#16858,#16859,#16860,#16861,#16862,#16863,#16864,
#16865,#16866,#16867,#16868,#16869,#16870,#16871,#16872,#16873,#16874,#16875,
#16876,#16877,#16878,#16879,#16880,#16881,#16882,#16883,#16884,#16885,#16886,
#16887,#16888,#16889,#16890,#16891,#16892,#16893,#16894,#16895,#16896,#16897,
#16898,#16899,#16900,#16901,#16902,#16903,#16904,#16905,#16906,#16907,#16908,
#16909,#16910,#16911,#16912,#16913,#16914,#16915,#16916,#16917,#16918,#16919,
#16920,#16921,#16922,#16923,#16924,#16925,#16926,#16927,#16928,#16929,#16930,
#16931,#16932,#16933,#16934,#16935,#16936,#16937,#16938,#16939,#16940,#16941,
#16942,#16943,#16944,#16945,#16946,#16947,#16948,#16949,#16950,#16951,#16952,
#16953,#16954,#16955,#16956,#16957,#16958,#16959,#16960,#16961,#16962,#16963,
#16964,#16965,#16966,#16967,#16968,#16969,#16970,#16971,#16972,#16973,#16974,
#16975,#16976,#16977,#16978,#16979,#16980,#16981,#16982,#16983,#16984,#16985,
#16986,#16987,#16988,#16989,#16990,#16991,#16992,#16993,#16994,#16995,#16996,
#16997,#16998,#16999,#17000,#17001,#17002,#17003,#17004,#17005,#17006,#17007,
#17008,#17009,#17010,#17011,#17012,#17013,#17014,#17015,#17016,#17017,#17018,
#17019,#17020,#17021,#17022,#17023,#17024,#17025,#17026,#17027,#17028,#17029,
#17030,#17031,#17032,#17033,#17034,#17035,#17036,#17037,#17038,#17039,#17040,
#17041,#17042,#17043,#17044,#17045,#17046,#17047,#17048,#17049,#17050,#17051,
#17052,#17053,#17054,#17055,#17056,#17057,#17058,#17059,#17060,#17061,#17062,
#17063,#17064,#17065,#17066),.UNSPECIFIED.,.F.,.F.,(4,2,2,2,2,2,2,2,2,2,
2,2,2,2,2,2,2,2,2,2,2,2,2,2,2,2,2,2,2,2,2,2,2,2,2,2,2,2,2,2,2,2,2,2,2,2,
2,2,2,2,2,2,2,2,2,2,2,2,2,2,2,2,2,2,2,2,2,2,2,2,2,2,2,2,2,2,2,2,2,2,2,2,
2,2,2,2,2,2,2,2,2,2,2,2,2,2,2,2,2,2,2,2,2,2,2,2,2,2,2,2,2,2,2,2,2,2,2,2,
2,4),(-4.05916345069716,-4.04238701742415,-4.0412065698486,-4.04046692611738,
-4.03990742164276,-4.03937351232827,-4.03884440649689,-4.03812094878392,
-4.03668921855855,-4.02492401590026,-4.02166665959467,-4.01813823905508,
-3.9311910304044,-3.90169236769069,-3.88256796975933,-3.88004547504971,
-3.87877812076469,-3.87786552687871,-3.87689843295007,-3.87553689947498,
-3.87271854108454,-3.84257004358246,-3.75536061535205,-3.73490766426559,
-3.72432949815798,-3.72069292615289,-3.71903545146009,-3.71772750156719,
-3.71704540014503,-3.71648838763052,-3.71584320447735,-3.71474935093017,
-3.71079893284687,-3.70739428217192,-3.70626206387556,-3.7045076413685,
-3.65362265165293,-3.6484681959611,-3.64263023559689,-3.63591998347896,
-3.62805570770431,-3.61856255594855,-3.60648396660814,-3.56522070048555,
-3.55871926063678,-3.55687939890934,-3.55575954493738,-3.55474981667737,
-3.55346220331885,-3.55084015757565,-3.53494715461474,-3.53379878434067,
-3.5325852347665,-3.53117874568734,-3.52542289888392,-3.48073866948945,
-3.43153015691186,-3.41025156527975,-3.40111765815316,-3.39785158352882,
-3.39632032357312,-3.39509350441574,-3.39442924084434,-3.39388048678388,
-3.39330996719067,-3.39223860286589,-3.38860919490417,-3.38755019788473,
-3.30514201999507,-3.29444807927639,-3.28153437390937,-3.24232442513772,
-3.23816708976306,-3.23504939593596,-3.23366720607616,-3.23264360723344,
-3.23169407521747,-3.2303991361461,-3.22784720277224,-3.20710276626331,
-3.20384980220311,-3.12578467054706,-3.10057067855046,-3.08208610857851,
-3.07657532391301,-3.0743225768046,-3.07315613877911,-3.07242234778116,
-3.07174471321827,-3.07119520108778,-3.07063293801307,-3.06960254686128,
-3.06631667699852,-3.00983817987694,-2.96129739873415,-2.9199064471678,
-2.91339311804808,-2.91155203701303,-2.91043190081032,-2.90942221607034,
-2.90813506801497,-2.90551539111582,-2.88966969124545,-2.88842054088033,
-2.88721063871179,-2.88571490739149,-2.88030591338413,-2.86004764387467,
-2.7865337635708,-2.77343855903824,-2.75370065406698,-2.75156289485082,
-2.75043998084599,-2.74972443465644,-2.74906021157489,-2.74851140739545,
-2.74794109974639,-2.7468709075016,-2.74325209895275,-2.69174590048981),
 .UNSPECIFIED.);
#106=B_SPLINE_CURVE_WITH_KNOTS('',3,(#17072,#17073,#17074,#17075,#17076,
#17077,#17078,#17079,#17080,#17081,#17082,#17083,#17084,#17085,#17086,#17087,
#17088,#17089,#17090,#17091,#17092,#17093,#17094,#17095,#17096,#17097,#17098,
#17099,#17100,#17101,#17102,#17103,#17104,#17105,#17106,#17107,#17108,#17109,
#17110,#17111,#17112,#17113,#17114,#17115,#17116,#17117,#17118,#17119,#17120,
#17121,#17122,#17123,#17124,#17125,#17126,#17127,#17128,#17129,#17130,#17131,
#17132,#17133,#17134,#17135,#17136,#17137,#17138,#17139,#17140,#17141,#17142,
#17143,#17144,#17145,#17146,#17147,#17148,#17149,#17150,#17151,#17152,#17153,
#17154,#17155,#17156,#17157,#17158,#17159,#17160,#17161,#17162,#17163,#17164,
#17165,#17166,#17167,#17168,#17169,#17170,#17171,#17172,#17173,#17174,#17175,
#17176,#17177,#17178,#17179,#17180,#17181,#17182,#17183,#17184,#17185,#17186,
#17187,#17188,#17189,#17190,#17191,#17192,#17193,#17194,#17195,#17196,#17197,
#17198,#17199,#17200,#17201,#17202,#17203,#17204,#17205,#17206,#17207,#17208,
#17209,#17210,#17211,#17212,#17213,#17214,#17215,#17216,#17217,#17218,#17219,
#17220,#17221,#17222,#17223,#17224,#17225,#17226,#17227,#17228,#17229,#17230,
#17231,#17232,#17233,#17234,#17235,#17236,#17237,#17238,#17239),
 .UNSPECIFIED.,.F.,.F.,(4,2,2,2,2,2,2,2,2,2,2,2,2,2,2,2,2,2,2,2,2,2,2,2,
2,2,2,2,2,2,2,2,2,2,2,2,2,2,2,2,2,2,2,2,2,2,2,2,2,2,2,2,2,2,2,2,2,2,2,2,
2,2,2,2,2,2,2,2,2,2,2,2,2,2,2,2,2,2,2,2,2,2,2,4),(-1.37002790224387,-1.29458298591376,
-1.28832508550233,-1.2864304459289,-1.28541121093775,-1.28442747248207,
-1.28324781545256,-1.28198537890397,-1.28002551568158,-1.27634808511337,
-1.24443219341799,-1.17754373071881,-1.12805991616991,-1.12519837762381,
-1.12422299783737,-1.123671630036,-1.12316495861639,-1.12247314039283,-1.12113598052038,
-1.11256179051614,-1.09266919370706,-1.0374060098776,-0.969107684862878,
-0.964884191471012,-0.963269402451135,-0.962306094948808,-0.961310768302774,
-0.960013783520247,-0.95858897723759,-0.956242509914642,-0.95153904273292,
-0.902399762192698,-0.807554643742085,-0.802637298308287,-0.801555880602724,
-0.800855951415351,-0.800294795385586,-0.799650287599147,-0.798532176764302,
-0.793878024485553,-0.770703558316142,-0.717435588570115,-0.686797711688131,
-0.644875675102968,-0.641561826201076,-0.640250351806751,-0.639296066098815,
-0.638294730544241,-0.636966622950325,-0.635498860213016,-0.633049327612804,
-0.628063681706848,-0.615089653853534,-0.584469575245545,-0.490284224177784,
-0.48019066509845,-0.478668854023999,-0.477947241727922,-0.477382413841213,
-0.476758334024105,-0.475731953869423,-0.472101190199959,-0.39060262223377,
-0.36530153366235,-0.321837415997487,-0.318498418093149,-0.317182581462893,
-0.316227074300268,-0.315226251145087,-0.313901775479984,-0.312439146319131,
-0.310002126542875,-0.305051208421974,-0.249972416504298,-0.16121522939384,
-0.156532897892942,-0.155470365242569,-0.154776212944072,-0.154271385927652,
-0.153641949625458,-0.152591867695583,-0.148721055014533,-0.0601448328895587,
-0.000961830990748762),.UNSPECIFIED.);
#107=B_SPLINE_CURVE_WITH_KNOTS('',3,(#17240,#17241,#17242,#17243,#17244,
#17245,#17246,#17247,#17248,#17249,#17250,#17251,#17252,#17253,#17254,#17255,
#17256,#17257,#17258,#17259,#17260,#17261,#17262,#17263,#17264,#17265,#17266,
#17267,#17268,#17269,#17270,#17271,#17272,#17273,#17274,#17275,#17276,#17277,
#17278,#17279,#17280,#17281,#17282,#17283,#17284,#17285,#17286,#17287,#17288,
#17289,#17290,#17291,#17292,#17293,#17294,#17295,#17296,#17297,#17298,#17299,
#17300,#17301,#17302,#17303,#17304,#17305,#17306,#17307,#17308,#17309,#17310,
#17311,#17312,#17313,#17314,#17315,#17316,#17317,#17318,#17319,#17320,#17321,
#17322,#17323,#17324,#17325,#17326,#17327,#17328,#17329,#17330,#17331,#17332,
#17333,#17334,#17335,#17336,#17337,#17338,#17339,#17340,#17341,#17342,#17343,
#17344,#17345,#17346,#17347),.UNSPECIFIED.,.F.,.F.,(4,2,2,2,2,2,2,2,2,2,
2,2,2,2,2,2,2,2,2,2,2,2,2,2,2,2,2,2,2,2,2,2,2,2,2,2,2,2,2,2,2,2,2,2,2,2,
2,2,2,2,2,2,2,4),(-4.06190468854636,-4.05761219415629,-4.05608881464177,
-4.05500854406393,-4.05406745855219,-4.05308867736803,-4.05178374552866,
-4.04968755611875,-4.04315095466864,-3.92840391957809,-3.90419065775357,
-3.89459214996301,-3.89321725719404,-3.89251757875117,-3.892009953747,-3.89146225608665,
-3.89050521829901,-3.88777302654306,-3.8453969310288,-3.78760225529129,
-3.74109176150481,-3.73651688209514,-3.73421771582856,-3.73281262704672,
-3.73152999954154,-3.73053584087752,-3.72956741803743,-3.72820254100494,
-3.72456322827935,-3.66534941440886,-3.6349238978713,-3.61149141065625,
-3.57322864657244,-3.57083416967513,-3.56995760052672,-3.56936673100346,
-3.56879327548793,-3.5681016143232,-3.56637326683988,-3.5504562188279,-3.54491878933992,
-3.52870610568813,-3.50950837695847,-3.46487134489713,-3.41829829944362,
-3.4137201847873,-3.41141981631327,-3.41001422015431,-3.40873113336743,
-3.40773691935731,-3.40676859542921,-3.40540410820989,-3.40257565754072,
-3.40092133460055),.UNSPECIFIED.);
#108=B_SPLINE_CURVE_WITH_KNOTS('',3,(#17348,#17349,#17350,#17351,#17352,
#17353,#17354,#17355,#17356,#17357,#17358,#17359,#17360,#17361,#17362,#17363,
#17364,#17365,#17366,#17367,#17368,#17369,#17370,#17371,#17372,#17373,#17374,
#17375,#17376,#17377,#17378,#17379,#17380,#17381,#17382,#17383,#17384,#17385,
#17386,#17387,#17388,#17389,#17390,#17391,#17392,#17393,#17394,#17395,#17396,
#17397,#17398,#17399,#17400,#17401,#17402,#17403,#17404,#17405,#17406,#17407,
#17408,#17409,#17410,#17411,#17412,#17413,#17414,#17415,#17416,#17417,#17418,
#17419,#17420,#17421,#17422,#17423,#17424,#17425,#17426,#17427,#17428,#17429,
#17430,#17431,#17432,#17433,#17434,#17435,#17436,#17437,#17438,#17439,#17440,
#17441,#17442,#17443,#17444,#17445,#17446,#17447,#17448,#17449,#17450,#17451,
#17452,#17453,#17454,#17455,#17456,#17457,#17458,#17459,#17460,#17461,#17462,
#17463,#17464,#17465,#17466,#17467,#17468,#17469,#17470,#17471,#17472,#17473,
#17474,#17475,#17476,#17477,#17478,#17479,#17480,#17481,#17482,#17483,#17484,
#17485,#17486,#17487,#17488,#17489,#17490,#17491,#17492,#17493,#17494,#17495,
#17496,#17497,#17498,#17499,#17500,#17501,#17502,#17503,#17504,#17505,#17506,
#17507,#17508,#17509,#17510,#17511,#17512,#17513,#17514,#17515,#17516,#17517,
#17518,#17519,#17520,#17521,#17522,#17523,#17524,#17525,#17526,#17527,#17528,
#17529,#17530,#17531,#17532,#17533,#17534,#17535,#17536,#17537,#17538,#17539,
#17540,#17541,#17542,#17543,#17544,#17545,#17546,#17547,#17548,#17549,#17550,
#17551,#17552,#17553,#17554,#17555,#17556,#17557,#17558,#17559,#17560,#17561,
#17562,#17563,#17564,#17565,#17566,#17567,#17568,#17569,#17570,#17571,#17572,
#17573,#17574,#17575,#17576,#17577,#17578,#17579,#17580,#17581,#17582,#17583,
#17584,#17585,#17586,#17587,#17588,#17589,#17590,#17591,#17592,#17593,#17594,
#17595,#17596,#17597,#17598,#17599,#17600,#17601,#17602,#17603,#17604,#17605,
#17606,#17607,#17608,#17609),.UNSPECIFIED.,.F.,.F.,(4,2,2,2,2,2,2,2,2,2,
2,2,2,2,2,2,2,2,2,2,2,2,2,2,2,2,2,2,2,2,2,2,2,2,2,2,2,2,2,2,2,2,2,2,2,2,
2,2,2,2,2,2,2,2,2,2,2,2,2,2,2,2,2,2,2,2,2,2,2,2,2,2,2,2,2,2,2,2,2,2,2,2,
2,2,2,2,2,2,2,2,2,2,2,2,2,2,2,2,2,2,2,2,2,2,2,2,2,2,2,2,2,2,2,2,2,2,2,2,
2,2,2,2,2,2,2,2,2,2,2,2,4),(-2.69174590048981,-2.68518422100538,-2.64003823633685,
-2.60659309213456,-2.59169192256623,-2.58931503417848,-2.58807770775278,
-2.58707267938913,-2.58606882256754,-2.58424911351925,-2.57859487991175,
-2.57414315645939,-2.57259213429865,-2.57085753983321,-2.56936317190141,
-2.56729950316768,-2.56617916488438,-2.56300960283324,-2.55676670780608,
-2.46584600275137,-2.44568437236955,-2.43038560345629,-2.42854262904682,
-2.42753364084114,-2.42686589087765,-2.42625938040751,-2.42575546550729,
-2.42517968100698,-2.42408247907887,-2.42022300962866,-2.35746791911276,
-2.33192924551851,-2.30190752123575,-2.28205772270088,-2.26881662806319,
-2.26651231815674,-2.26529023771498,-2.26428597610859,-2.26327306724939,
-2.2614088962616,-2.25540154310491,-2.13960846954174,-2.11515924678835,
-2.10550346585773,-2.10412673045116,-2.10342671501855,-2.1028656719539,
-2.10222149556217,-2.10113278542222,-2.09723415042546,-2.03121125257412,
-1.94981376148369,-1.94470382150031,-1.94295686441705,-1.94196743686215,
-1.94106038615009,-1.93984104290258,-1.93755021816621,-1.9245975184417,
-1.90010143480742,-1.81074963803791,-1.78343885676484,-1.78150762229552,
-1.78076242818885,-1.78022740943251,-1.77965787522611,-1.7788912910346,
-1.77717256811746,-1.73327966500754,-1.62812175692323,-1.62192907899042,
-1.62004235066097,-1.61902480023222,-1.61811763844147,-1.61698630835668,
-1.61577111044837,-1.61392312457034,-1.58992061227593,-1.56817641336249,
-1.51750027515747,-1.46219421320072,-1.45897098851102,-1.45794828032615,
-1.45738743478175,-1.45682643179475,-1.45612636192972,-1.45474918525135,
-1.44507755445118,-1.42056623661874,-1.30489392770242,-1.29889587327511,
-1.29703291311642,-1.29602029151251,-1.29503615893875,-1.29384711139481,
-1.29257162773646,-1.29058045929385,-1.2499399174154,-1.14391045076237,
-1.13646078816555,-1.13521411609317,-1.13447205707712,-1.13390442655053,
-1.13329081492958,-1.1323103301683,-1.12910432393532,-1.0808283994584,-1.02077805548855,
-0.978429817451106,-0.975109792652688,-0.973797522204595,-0.97284322924698,
-0.971842478659921,-0.970518016291771,-0.96905340597356,-0.966611113498652,
-0.913842469785866,-0.818160693128627,-0.813241130670578,-0.812159624357048,
-0.811459713751008,-0.810898623380081,-0.810254246866453,-0.809136500887032,
-0.804485742183531,-0.781021794947152,-0.765140823279486,-0.753974165049035,
-0.744311195506223,-0.685210091495683,-0.66212538598945),.UNSPECIFIED.);
#109=B_SPLINE_CURVE_WITH_KNOTS('',3,(#17614,#17615,#17616,#17617,#17618,
#17619,#17620,#17621,#17622,#17623,#17624,#17625,#17626,#17627,#17628,#17629,
#17630,#17631,#17632,#17633,#17634,#17635,#17636,#17637,#17638,#17639,#17640,
#17641,#17642,#17643,#17644,#17645,#17646,#17647,#17648,#17649,#17650,#17651,
#17652,#17653,#17654,#17655,#17656,#17657,#17658,#17659,#17660,#17661,#17662,
#17663,#17664,#17665,#17666,#17667,#17668,#17669,#17670,#17671,#17672,#17673,
#17674,#17675,#17676,#17677,#17678,#17679,#17680,#17681,#17682,#17683,#17684,
#17685,#17686,#17687,#17688,#17689,#17690,#17691,#17692,#17693,#17694,#17695,
#17696,#17697,#17698,#17699,#17700,#17701,#17702,#17703,#17704,#17705,#17706,
#17707,#17708,#17709,#17710,#17711,#17712,#17713,#17714,#17715,#17716,#17717,
#17718,#17719,#17720,#17721,#17722,#17723,#17724,#17725,#17726,#17727,#17728,
#17729,#17730,#17731,#17732,#17733,#17734,#17735,#17736,#17737,#17738,#17739,
#17740,#17741,#17742,#17743,#17744,#17745,#17746,#17747,#17748,#17749,#17750,
#17751,#17752,#17753,#17754,#17755,#17756,#17757,#17758,#17759,#17760,#17761,
#17762,#17763,#17764,#17765,#17766,#17767,#17768,#17769,#17770,#17771,#17772,
#17773,#17774,#17775,#17776,#17777,#17778,#17779,#17780,#17781,#17782,#17783,
#17784,#17785,#17786,#17787,#17788,#17789,#17790,#17791,#17792,#17793,#17794,
#17795,#17796,#17797,#17798,#17799,#17800,#17801,#17802,#17803,#17804,#17805,
#17806,#17807,#17808,#17809,#17810,#17811,#17812,#17813,#17814,#17815,#17816,
#17817,#17818,#17819,#17820,#17821,#17822,#17823,#17824,#17825,#17826,#17827,
#17828,#17829,#17830,#17831,#17832,#17833,#17834,#17835,#17836,#17837,#17838,
#17839,#17840,#17841,#17842,#17843,#17844,#17845,#17846,#17847,#17848,#17849,
#17850,#17851,#17852,#17853,#17854,#17855,#17856,#17857,#17858,#17859,#17860,
#17861,#17862,#17863,#17864,#17865,#17866,#17867,#17868,#17869,#17870,#17871,
#17872,#17873,#17874,#17875,#17876,#17877,#17878,#17879,#17880,#17881,#17882,
#17883,#17884,#17885,#17886,#17887,#17888,#17889,#17890,#17891,#17892,#17893,
#17894,#17895,#17896,#17897,#17898,#17899,#17900,#17901,#17902,#17903,#17904,
#17905,#17906,#17907),.UNSPECIFIED.,.F.,.F.,(4,2,2,2,2,2,2,2,2,2,2,2,2,
2,2,2,2,2,2,2,2,2,2,2,2,2,2,2,2,2,2,2,2,2,2,2,2,2,2,2,2,2,2,2,2,2,2,2,2,
2,2,2,2,2,2,2,2,2,2,2,2,2,2,2,2,2,2,2,2,2,2,2,2,2,2,2,2,2,2,2,2,2,2,2,2,
2,2,2,2,2,2,2,2,2,2,2,2,2,2,2,2,2,2,2,2,2,2,2,2,2,2,2,2,2,2,2,2,2,2,2,2,
2,2,2,2,2,2,2,2,2,2,2,2,2,2,2,2,2,2,2,2,2,2,2,2,2,4),(-3.39964611755361,
-3.39764880888014,-3.39028359886401,-3.38749424433923,-3.38550393410291,
-3.38469269291067,-3.38416690616382,-3.38359400042095,-3.38290404404684,
-3.38118540884625,-3.36559581815718,-3.36436761100055,-3.28070406807476,
-3.24304656119502,-3.22703271126754,-3.22461221137527,-3.22336563749605,
-3.22236898473675,-3.22122623484675,-3.21928478740514,-3.21261766559457,
-3.20881186389429,-3.20714389248125,-3.20505499277876,-3.20449832602741,
-3.20241085374811,-3.20095249922505,-3.1997471079553,-3.1984230487437,-3.1922863270394,
-3.10163115893095,-3.07529061139275,-3.06757581273616,-3.06468977181308,
-3.06329156039486,-3.06246134374105,-3.0617143696158,-3.06115588937341,
-3.06062177726627,-3.05987976564568,-3.05796726431532,-3.03180746501154,
-3.01888433749514,-2.95560870912241,-2.92423949613558,-2.90440753338004,
-2.9018638478,-2.90059180591221,-2.89967818185691,-2.89871216321321,-2.89735567976228,
-2.89455921559808,-2.86537843065831,-2.82456358735152,-2.76628710912738,
-2.74377472923209,-2.74146478104603,-2.74027675049345,-2.73953382822886,
-2.73885060380401,-2.73830037251212,-2.7377417052022,-2.73672975184566,
-2.73359093184269,-2.68277282211097,-2.61870836531877,-2.59392326861083,
-2.5812015010272,-2.57892208010584,-2.57770520857356,-2.57670105134096,
-2.57568468361527,-2.57380378207173,-2.5676596352238,-2.45877194550658,
-2.4191061799309,-2.41763814338397,-2.41677924292446,-2.41601039439534,
-2.41544842557432,-2.41491941479278,-2.41419714142552,-2.41277092951605,
-2.40118202915324,-2.35737506413223,-2.32944818877692,-2.29845856239273,
-2.25953607015129,-2.25642151629098,-2.25503938725787,-2.25401530686515,
-2.25306495253363,-2.25176831283154,-2.24921129294349,-2.22835565554174,
-2.22529473950393,-2.14729337158211,-2.12201290518429,-2.10337701005734,
-2.09502276808912,-2.0936943728541,-2.09300435900876,-2.09244390443422,
-2.09187718836772,-2.09082582177403,-2.08737088277271,-2.03160578560812,
-1.93986722104493,-1.93435358872919,-1.93255166984769,-1.93155110640454,
-1.93055470128873,-1.9293143747895,-1.92692480416711,-1.91172902694223,
-1.87715650469911,-1.78508051585075,-1.78446470697245,-1.77239739388375,
-1.77079491512526,-1.77005798632339,-1.7694910321886,-1.76887481618364,
-1.76788318212385,-1.76457926095916,-1.74402529726688,-1.72000062346364,
-1.61745201802918,-1.6113913106676,-1.60952027060051,-1.60850577276141,
-1.60752139961626,-1.60633420674337,-1.60506146114842,-1.6030771863552,
-1.59933660911843,-1.56650360112663,-1.47701329868817,-1.44984351680212,
-1.4479143038609,-1.44716938464344,-1.44663439303519,-1.44606472260467,
-1.44529767900208,-1.44357678235006,-1.39885146808684,-1.37002790224387),
 .UNSPECIFIED.);
#110=B_SPLINE_CURVE_WITH_KNOTS('',3,(#17909,#17910,#17911,#17912,#17913,
#17914,#17915,#17916,#17917,#17918,#17919,#17920,#17921,#17922,#17923,#17924,
#17925,#17926,#17927,#17928,#17929,#17930,#17931,#17932,#17933,#17934,#17935,
#17936,#17937,#17938,#17939,#17940,#17941,#17942,#17943,#17944,#17945,#17946,
#17947,#17948,#17949,#17950,#17951,#17952,#17953,#17954,#17955,#17956,#17957,
#17958,#17959,#17960,#17961,#17962,#17963,#17964,#17965,#17966,#17967,#17968,
#17969,#17970,#17971,#17972,#17973,#17974,#17975,#17976,#17977,#17978,#17979,
#17980,#17981,#17982,#17983,#17984,#17985,#17986,#17987,#17988,#17989,#17990,
#17991,#17992,#17993,#17994,#17995,#17996,#17997,#17998,#17999,#18000,#18001,
#18002,#18003,#18004,#18005,#18006,#18007,#18008,#18009,#18010,#18011,#18012),
 .UNSPECIFIED.,.F.,.F.,(4,2,2,2,2,2,2,2,2,2,2,2,2,2,2,2,2,2,2,2,2,2,2,2,
2,2,2,2,2,2,2,2,2,2,2,2,2,2,2,2,2,2,2,2,2,2,2,2,2,2,2,4),(-0.66212538598945,
-0.655149255888499,-0.652080313642583,-0.650811460957387,-0.649868153424591,
-0.648859619637481,-0.647488713627128,-0.645961473694271,-0.635908521032501,
-0.617069796067174,-0.593499644285835,-0.505001047530479,-0.504025019200631,
-0.503623336120885,-0.502843125226789,-0.490998101015034,-0.489562816761166,
-0.488838174162473,-0.488308493585097,-0.487735247959456,-0.486947537252467,
-0.48511130522012,-0.440577912753107,-0.417866669091863,-0.388735385598929,
-0.332843740543996,-0.329358827539456,-0.328018773799749,-0.32705692603359,
-0.326059655065999,-0.324756717039751,-0.323323765517538,-0.32095798966878,
-0.274723435099736,-0.171670772576037,-0.170995440758908,-0.167137915343662,
-0.16604039123246,-0.165464260407457,-0.164960166302212,-0.164307311623509,
-0.163151992707949,-0.158007635387551,-0.104186532232884,-0.0435463687287092,
-0.0107744231480432,-0.00654643351052616,-0.00493057774174045,-0.00396677176403925,
-0.00299633523756008,-0.00201057957694441,-0.000961474156681484),
 .UNSPECIFIED.);
#111=B_SPLINE_CURVE_WITH_KNOTS('',3,(#18013,#18014,#18015,#18016,#18017,
#18018,#18019,#18020,#18021,#18022,#18023,#18024,#18025,#18026,#18027,#18028,
#18029,#18030,#18031,#18032,#18033,#18034,#18035,#18036,#18037,#18038,#18039,
#18040,#18041,#18042,#18043,#18044,#18045,#18046,#18047,#18048,#18049,#18050,
#18051,#18052,#18053,#18054,#18055,#18056,#18057,#18058,#18059,#18060,#18061,
#18062,#18063,#18064,#18065,#18066,#18067,#18068,#18069,#18070,#18071,#18072,
#18073,#18074,#18075,#18076,#18077,#18078,#18079,#18080,#18081,#18082,#18083,
#18084,#18085,#18086,#18087,#18088,#18089,#18090,#18091,#18092,#18093,#18094,
#18095,#18096,#18097,#18098,#18099,#18100,#18101,#18102,#18103,#18104,#18105,
#18106,#18107,#18108,#18109,#18110,#18111,#18112,#18113,#18114,#18115,#18116,
#18117,#18118,#18119,#18120,#18121,#18122,#18123,#18124,#18125,#18126,#18127,
#18128,#18129,#18130,#18131,#18132,#18133,#18134,#18135,#18136,#18137,#18138,
#18139,#18140,#18141,#18142,#18143,#18144,#18145,#18146,#18147,#18148,#18149,
#18150,#18151,#18152,#18153,#18154,#18155,#18156,#18157,#18158,#18159,#18160,
#18161,#18162,#18163,#18164,#18165,#18166,#18167,#18168,#18169,#18170,#18171,
#18172,#18173,#18174,#18175,#18176,#18177,#18178,#18179,#18180,#18181,#18182,
#18183,#18184,#18185,#18186,#18187,#18188,#18189,#18190,#18191,#18192,#18193,
#18194,#18195,#18196,#18197,#18198,#18199,#18200,#18201,#18202,#18203,#18204,
#18205,#18206,#18207,#18208,#18209,#18210,#18211,#18212,#18213,#18214,#18215,
#18216,#18217,#18218,#18219,#18220,#18221,#18222,#18223,#18224,#18225,#18226,
#18227,#18228,#18229,#18230,#18231,#18232,#18233,#18234,#18235,#18236,#18237,
#18238,#18239,#18240,#18241,#18242,#18243,#18244,#18245,#18246,#18247,#18248,
#18249,#18250,#18251,#18252,#18253,#18254,#18255,#18256,#18257,#18258,#18259,
#18260,#18261,#18262,#18263,#18264,#18265,#18266,#18267,#18268,#18269,#18270,
#18271,#18272,#18273,#18274,#18275,#18276,#18277,#18278,#18279,#18280,#18281,
#18282,#18283,#18284,#18285,#18286,#18287,#18288,#18289,#18290,#18291,#18292,
#18293,#18294,#18295,#18296,#18297,#18298,#18299,#18300,#18301,#18302,#18303,
#18304,#18305,#18306,#18307,#18308,#18309,#18310,#18311,#18312,#18313,#18314,
#18315,#18316,#18317,#18318,#18319,#18320),.UNSPECIFIED.,.F.,.F.,(4,2,2,
2,2,2,2,2,2,2,2,2,2,2,2,2,2,2,2,2,2,2,2,2,2,2,2,2,2,2,2,2,2,2,2,2,2,2,2,
2,2,2,2,2,2,2,2,2,2,2,2,2,2,2,2,2,2,2,2,2,2,2,2,2,2,2,2,2,2,2,2,2,2,2,2,
2,2,2,2,2,2,2,2,2,2,2,2,2,2,2,2,2,2,2,2,2,2,2,2,2,2,2,2,2,2,2,2,2,2,2,2,
2,2,2,2,2,2,2,2,2,2,2,2,2,2,2,2,2,2,2,2,2,2,2,2,2,2,2,2,2,2,2,2,2,2,2,2,
2,2,2,2,2,2,4),(-4.06013899922515,-4.0586875745572,-4.05295619445666,-3.99595432886195,
-3.90743304213108,-3.90366172672679,-3.9026234205714,-3.90199788786373,
-3.90143561105364,-3.90071047995764,-3.89920370627736,-3.88936904934743,
-3.88684592202701,-3.81217450881903,-3.74707911988152,-3.74334802637265,
-3.7422113591884,-3.74112176452309,-3.74111999729241,-3.74111822680033,
-3.7411164531622,-3.74111467572886,-3.7411128952234,-3.74111111147165,-3.74110932534831,
-3.74110753614702,-3.7411057433825,-3.74110394773589,-3.74110214858439,
-3.74110034609982,-3.7410985400745,-3.74109673033107,-3.74109491721153,
-3.74109310051361,-3.74109128002891,-3.74108945631834,-3.74108762903612,
-3.74108579803414,-3.74108396384155,-3.74108212583386,-3.74108028448055,
-3.74107843874733,-3.7410765893995,-3.74107473673564,-3.74107288051646,
-3.74107102081256,-3.74106915737625,-3.74106729018932,-3.74106541859219,
-3.74106354290762,-3.74106166315262,-3.74105977868544,-3.74105789078802,
-3.74105599908219,-3.74105410274061,-3.74105220305217,-3.74105029914567,
-3.74104751496156,-3.74104470505104,-3.7410418684829,-3.74103900455023,
-3.74103611326526,-3.74103319465499,-3.74103024734447,-3.74102727051948,
-3.74102426449811,-3.74102122826827,-3.74101816106587,-3.7410150623111,
-3.74101193147574,-3.74100876844032,-3.74100557245444,-3.74100234234137,
-3.74099907762704,-3.74099577750281,-3.74099244148926,-3.7409890683824,
-3.74098565787669,-3.74098220890591,-3.74097872100004,-3.74097519287914,
-3.74097162372978,-3.74096801278414,-3.74096435879223,-3.74096066129493,
-3.74095691891617,-3.74095313081701,-3.74094929622517,-3.74094332869619,
-3.74093704221519,-3.74093041375631,-3.7409234120281,-3.7399139229473,-3.73854382662273,
-3.73553411410434,-3.70768162913358,-3.62007844788081,-3.60552854608082,
-3.58442644552575,-3.58106949416065,-3.58007204741027,-3.57945453703141,
-3.57888801313887,-3.57815385954381,-3.57656605164298,-3.5648825007658,
-3.56232404342509,-3.56027754174261,-3.4619521364563,-3.42279275873346,
-3.4199305806262,-3.41861253167617,-3.41761323426829,-3.4166563244859,-3.41513103219056,
-3.41126264148037,-3.34847176150003,-3.26355811940794,-3.25831745488997,
-3.25715554793509,-3.25650136437895,-3.25599739509,-3.25542264390492,-3.25433144278923,
-3.25052967342322,-3.24977986530622,-3.14697028190909,-3.11377686894825,
-3.09893687628056,-3.09656165651435,-3.09534132874385,-3.09435504983365,
-3.09321443905326,-3.09136357056326,-3.08515666266749,-2.98167556854355,
-2.93982136656069,-2.9350954318702,-2.93397165273407,-2.93332588423217,
-2.9327648558476,-2.93206666100736,-2.93099082796192,-2.92614329445909,
-2.82980065311447,-2.79195551304572,-2.77588988085229,-2.77346676628664,
-2.77223640868239,-2.77124893766084,-2.77025857221109,-2.76857508300121,
-2.76367198214429,-2.69189203107631),.UNSPECIFIED.);
#112=B_SPLINE_CURVE_WITH_KNOTS('',3,(#18326,#18327,#18328,#18329,#18330,
#18331,#18332,#18333,#18334,#18335,#18336,#18337,#18338,#18339,#18340,#18341,
#18342,#18343,#18344,#18345,#18346,#18347,#18348,#18349,#18350,#18351,#18352,
#18353,#18354,#18355,#18356,#18357,#18358,#18359,#18360,#18361,#18362,#18363,
#18364,#18365,#18366,#18367,#18368,#18369,#18370,#18371,#18372,#18373,#18374,
#18375,#18376,#18377,#18378,#18379,#18380,#18381,#18382,#18383,#18384,#18385,
#18386,#18387,#18388,#18389,#18390,#18391,#18392,#18393,#18394,#18395,#18396,
#18397,#18398,#18399,#18400,#18401,#18402,#18403,#18404,#18405,#18406,#18407,
#18408,#18409,#18410,#18411,#18412,#18413,#18414,#18415,#18416,#18417,#18418,
#18419,#18420,#18421,#18422,#18423,#18424,#18425,#18426,#18427,#18428,#18429,
#18430,#18431,#18432,#18433,#18434,#18435,#18436,#18437,#18438,#18439,#18440,
#18441,#18442,#18443,#18444,#18445,#18446,#18447,#18448,#18449,#18450,#18451,
#18452,#18453,#18454,#18455,#18456,#18457,#18458,#18459,#18460,#18461,#18462,
#18463,#18464,#18465,#18466,#18467,#18468,#18469,#18470,#18471,#18472,#18473,
#18474,#18475,#18476,#18477,#18478,#18479,#18480,#18481,#18482,#18483,#18484,
#18485,#18486,#18487,#18488,#18489,#18490,#18491,#18492,#18493,#18494,#18495,
#18496,#18497,#18498,#18499,#18500,#18501,#18502,#18503,#18504,#18505,#18506,
#18507,#18508,#18509,#18510,#18511,#18512,#18513,#18514,#18515,#18516,#18517,
#18518,#18519,#18520,#18521,#18522,#18523,#18524,#18525,#18526,#18527),
 .UNSPECIFIED.,.F.,.F.,(4,2,2,2,2,2,2,2,2,2,2,2,2,2,2,2,2,2,2,2,2,2,2,2,
2,2,2,2,2,2,2,2,2,2,2,2,2,2,2,2,2,2,2,2,2,2,2,2,2,2,2,2,2,2,2,2,2,2,2,2,
2,2,2,2,2,2,2,2,2,2,2,2,2,2,2,2,2,2,2,2,2,2,2,2,2,2,2,2,2,2,2,2,2,2,2,2,
2,2,2,2,4),(-1.37062515302182,-1.36641565482268,-1.27609363253147,-1.26562488983865,
-1.26423972759399,-1.26352783689801,-1.26300133782122,-1.26247372834128,
-1.26171841145412,-1.26087668762849,-1.25945086169902,-1.22444716232454,
-1.13858179229422,-1.10688293184699,-1.10377375487603,-1.10249756865072,
-1.10155223976081,-1.10052393330455,-1.09911889985823,-1.09587804837423,
-1.04675590837091,-0.946551994728326,-0.941859909657036,-0.940796500239114,
-0.940102038450828,-0.939575187889014,-0.93895137279626,-0.937907271255098,
-0.936650218564192,-0.934155066534423,-0.927827521204583,-0.899425032528053,
-0.808650900285716,-0.802532597614302,-0.801173537062347,-0.799964094549804,
-0.798665305579509,-0.782832549823992,-0.780211716714131,-0.778923583851746,
-0.777912934643645,-0.776791531014876,-0.774947915245976,-0.768421086683194,
-0.726905038828855,-0.68406974733959,-0.624696442346727,-0.622925876576024,
-0.618703690967211,-0.617581295242227,-0.616929046836719,-0.616424022140671,
-0.615771846088075,-0.614600359435976,-0.613154372708063,-0.610134125503863,
-0.601928887601961,-0.580910874897554,-0.464140372440386,-0.458268274441317,
-0.456420165562351,-0.455410135141127,-0.454405001029571,-0.453176438344879,
-0.450843551000649,-0.43700154314809,-0.408941259757973,-0.364818871370853,
-0.344159311728564,-0.314840045020435,-0.31358851248783,-0.310477109160586,
-0.308256695420992,-0.296314855252144,-0.294717055376978,-0.29398097973713,
-0.293414127242867,-0.292889086160957,-0.29199968528913,-0.289517197510724,
-0.285822258016314,-0.275015586313579,-0.255279241027809,-0.171671402440776,
-0.159356029159895,-0.157289607043008,-0.15350026880912,-0.152476312074276,
-0.150374446373386,-0.14988330362345,-0.146282643557815,-0.142688989105406,
-0.135623691065618,-0.133661519840756,-0.132502387149721,-0.131597772448471,
-0.130411008793144,-0.128271970319934,-0.118055918508685,-0.0988087748871246,
-0.000962583817212411),.UNSPECIFIED.);
#113=B_SPLINE_CURVE_WITH_KNOTS('',3,(#18528,#18529,#18530,#18531,#18532,
#18533,#18534,#18535,#18536,#18537,#18538,#18539,#18540,#18541,#18542,#18543,
#18544,#18545,#18546,#18547,#18548,#18549,#18550,#18551,#18552,#18553,#18554,
#18555,#18556,#18557,#18558,#18559,#18560,#18561,#18562,#18563,#18564,#18565,
#18566,#18567,#18568,#18569,#18570,#18571,#18572,#18573,#18574,#18575,#18576,
#18577,#18578,#18579,#18580,#18581,#18582,#18583,#18584,#18585,#18586,#18587,
#18588,#18589,#18590,#18591,#18592,#18593,#18594,#18595,#18596,#18597,#18598,
#18599,#18600,#18601,#18602,#18603,#18604,#18605,#18606,#18607,#18608,#18609,
#18610,#18611,#18612,#18613,#18614,#18615,#18616,#18617,#18618,#18619,#18620,
#18621,#18622,#18623,#18624,#18625,#18626,#18627,#18628,#18629,#18630,#18631,
#18632,#18633),.UNSPECIFIED.,.F.,.F.,(4,2,2,2,2,2,2,2,2,2,2,2,2,2,2,2,2,
2,2,2,2,2,2,2,2,2,2,2,2,2,2,2,2,2,2,2,2,2,2,2,2,2,2,2,2,2,2,2,2,2,2,2,4),
(-4.06029665726298,-4.0330737903042,-4.03176370135331,-4.03096997183204,
-4.03039022437582,-4.02986449540016,-4.02929144962724,-4.02860060027115,
-4.02687594833907,-4.01106606720309,-4.00984336132231,-4.00852759203014,
-4.00163337731891,-3.99781065304034,-3.91009007232647,-3.88535200576533,
-3.87253178240235,-3.87024812020121,-3.86903061361906,-3.86802678392069,
-3.86701147475226,-3.86513465134125,-3.8590208814528,-3.74931545505425,
-3.72766723372853,-3.71721139895684,-3.71193257618668,-3.7097500843038,
-3.70811682592704,-3.70736822882574,-3.70683438297157,-3.7063054457511,
-3.70558295904313,-3.70415538162247,-3.69251660275401,-3.68146748042713,
-3.63725605826443,-3.63216025395095,-3.62630630478957,-3.61947666376359,
-3.61132656722799,-3.60122956298365,-3.56541335487771,-3.54988863808648,
-3.54748673218128,-3.54624405741294,-3.54523851754718,-3.54423732196841,
-3.54243126367529,-3.53688341933244,-3.44549490931712,-3.41522988039278,
-3.39964611755361),.UNSPECIFIED.);
#114=B_SPLINE_CURVE_WITH_KNOTS('',3,(#18634,#18635,#18636,#18637,#18638,
#18639,#18640,#18641,#18642,#18643,#18644,#18645,#18646,#18647,#18648,#18649,
#18650,#18651,#18652,#18653,#18654,#18655,#18656,#18657,#18658,#18659,#18660,
#18661,#18662,#18663,#18664,#18665,#18666,#18667,#18668,#18669,#18670,#18671,
#18672,#18673,#18674,#18675,#18676,#18677,#18678,#18679,#18680,#18681,#18682,
#18683,#18684,#18685,#18686,#18687,#18688,#18689,#18690,#18691,#18692,#18693,
#18694,#18695,#18696,#18697,#18698,#18699,#18700,#18701,#18702,#18703,#18704,
#18705,#18706,#18707,#18708,#18709,#18710,#18711,#18712,#18713,#18714,#18715,
#18716,#18717,#18718,#18719,#18720,#18721,#18722,#18723,#18724,#18725,#18726,
#18727,#18728,#18729,#18730,#18731,#18732,#18733,#18734,#18735,#18736,#18737,
#18738,#18739,#18740,#18741,#18742,#18743,#18744,#18745,#18746,#18747,#18748,
#18749,#18750,#18751,#18752,#18753,#18754,#18755,#18756,#18757,#18758,#18759,
#18760,#18761,#18762,#18763,#18764,#18765,#18766,#18767,#18768,#18769,#18770,
#18771,#18772,#18773,#18774,#18775,#18776,#18777,#18778,#18779,#18780,#18781,
#18782,#18783,#18784,#18785,#18786,#18787,#18788,#18789,#18790,#18791,#18792,
#18793,#18794,#18795,#18796,#18797,#18798,#18799,#18800,#18801,#18802,#18803,
#18804,#18805,#18806,#18807,#18808,#18809,#18810,#18811,#18812,#18813,#18814,
#18815,#18816,#18817,#18818,#18819,#18820,#18821,#18822,#18823,#18824,#18825,
#18826,#18827,#18828,#18829,#18830,#18831,#18832,#18833,#18834,#18835,#18836,
#18837,#18838,#18839,#18840,#18841,#18842,#18843,#18844,#18845,#18846,#18847,
#18848,#18849,#18850,#18851,#18852,#18853,#18854,#18855,#18856,#18857,#18858,
#18859,#18860,#18861,#18862,#18863,#18864,#18865,#18866,#18867,#18868,#18869,
#18870,#18871,#18872,#18873,#18874,#18875,#18876,#18877,#18878,#18879,#18880,
#18881,#18882,#18883,#18884,#18885,#18886,#18887,#18888,#18889,#18890,#18891,
#18892,#18893,#18894,#18895,#18896,#18897,#18898,#18899,#18900,#18901,#18902,
#18903,#18904,#18905,#18906,#18907,#18908,#18909,#18910,#18911,#18912,#18913,
#18914,#18915,#18916,#18917,#18918,#18919,#18920,#18921,#18922,#18923,#18924,
#18925),.UNSPECIFIED.,.F.,.F.,(4,2,2,2,2,2,2,2,2,2,2,2,2,2,2,2,2,2,2,2,
2,2,2,2,2,2,2,2,2,2,2,2,2,2,2,2,2,2,2,2,2,2,2,2,2,2,2,2,2,2,2,2,2,2,2,2,
2,2,2,2,2,2,2,2,2,2,2,2,2,2,2,2,2,2,2,2,2,2,2,2,2,2,2,2,2,2,2,2,2,2,2,2,
2,2,2,2,2,2,2,2,2,2,2,2,2,2,2,2,2,2,2,2,2,2,2,2,2,2,2,2,2,2,2,2,2,2,2,2,
2,2,2,2,2,2,2,2,2,2,2,2,2,2,2,2,2,4),(-2.69189203107631,-2.68428954741764,
-2.63577028753381,-2.62012960018365,-2.61238426504089,-2.61108192787796,
-2.61039739510307,-2.6098914560354,-2.60933626224789,-2.60851802068271,
-2.60610395742506,-2.564929278542,-2.55019284037311,-2.49941060665319,-2.4674509839559,
-2.45291320005841,-2.4505502910439,-2.44933256056893,-2.44834619326602,
-2.44734936719158,-2.44563610965843,-2.44051929215305,-2.35731338105497,
-2.33387149942606,-2.30254696645546,-2.29394201988924,-2.28918833002886,
-2.28806237545317,-2.28741611932471,-2.28685513184095,-2.28615758357564,
-2.28508384177392,-2.28026230880883,-2.18738861074219,-2.13083518514162,
-2.12785887366782,-2.12650217679043,-2.12548225021629,-2.12452506714646,
-2.12320233496673,-2.11982140322233,-2.07345579051452,-2.06198652144675,
-2.03063095140453,-1.97859342104963,-1.96698553589971,-1.96555859045138,
-1.96483610477134,-1.96430701420904,-1.96373341107364,-1.96294347934999,
-1.96109429151167,-1.91191506401489,-1.83699430017802,-1.80815237797425,
-1.80509441513226,-1.80383898566697,-1.80289900119436,-1.80186661256809,
-1.80043792556712,-1.79706030830855,-1.7924673930074,-1.74559642138161,
-1.64808388347933,-1.64797257560582,-1.64330978443652,-1.64224875224037,
-1.64155514277817,-1.64103102677971,-1.64048243994302,-1.63951645074417,
-1.6383746596351,-1.63618784648208,-1.61568724978367,-1.60246140939823,
-1.51467727485812,-1.48511456120563,-1.48230817638317,-1.48094901167397,
-1.47998205258638,-1.47906832841281,-1.47779740410006,-1.47526053726908,
-1.45569619747916,-1.42504224288354,-1.33340698606674,-1.3320666941687,
-1.32090461532728,-1.31935709805975,-1.31861956395952,-1.31805243699706,
-1.31744875566235,-1.31649056345389,-1.31536015107664,-1.31320336592572,
-1.29317967364103,-1.26115104658759,-1.20041699230803,-1.1831287740944,
-1.17777754742295,-1.17539535899219,-1.17483817482101,-1.16119885319424,
-1.15894813934127,-1.15761091405091,-1.15659017354175,-1.15550263120088,
-1.1538103739092,-1.14863280827768,-1.12009233516503,-1.07716178845513,
-1.0015082165501,-0.997263024023724,-0.996138404731537,-0.995485673245957,
-0.994936220794554,-0.994265637615803,-0.993541869054831,-0.992399879013481,
-0.990212659799501,-0.984919984839318,-0.974430455778944,-0.94830974808123,
-0.843058150211126,-0.836976675519868,-0.835102846831557,-0.834087635337282,
-0.833082943865943,-0.831863013735416,-0.829570716675205,-0.816600450796806,
-0.792142239192224,-0.777669894878879,-0.766654656886504,-0.682022446493819,
-0.67998888177348,-0.676202864791703,-0.673710969432534,-0.672789109668688,
-0.672248301687609,-0.671706309084773,-0.670986762361964,-0.669498760182229,
-0.667556852017813,-0.663051728732441,-0.661909204026248),.UNSPECIFIED.);
#115=B_SPLINE_CURVE_WITH_KNOTS('',3,(#18930,#18931,#18932,#18933,#18934,
#18935,#18936,#18937,#18938,#18939,#18940,#18941,#18942,#18943,#18944,#18945,
#18946,#18947,#18948,#18949,#18950,#18951,#18952,#18953,#18954,#18955,#18956,
#18957,#18958,#18959,#18960,#18961,#18962,#18963,#18964,#18965,#18966,#18967,
#18968,#18969,#18970,#18971,#18972,#18973,#18974,#18975,#18976,#18977,#18978,
#18979,#18980,#18981,#18982,#18983,#18984,#18985,#18986,#18987,#18988,#18989,
#18990,#18991,#18992,#18993,#18994,#18995,#18996,#18997,#18998,#18999,#19000,
#19001,#19002,#19003,#19004,#19005,#19006,#19007,#19008,#19009,#19010,#19011,
#19012,#19013,#19014,#19015,#19016,#19017,#19018,#19019,#19020,#19021,#19022,
#19023,#19024,#19025,#19026,#19027,#19028,#19029,#19030,#19031,#19032,#19033,
#19034,#19035,#19036,#19037,#19038,#19039,#19040,#19041,#19042,#19043,#19044,
#19045,#19046,#19047,#19048,#19049,#19050,#19051,#19052,#19053,#19054,#19055,
#19056,#19057,#19058,#19059,#19060,#19061,#19062,#19063,#19064,#19065,#19066,
#19067,#19068,#19069,#19070,#19071,#19072,#19073,#19074,#19075,#19076,#19077,
#19078,#19079,#19080,#19081,#19082,#19083,#19084,#19085,#19086,#19087,#19088,
#19089,#19090,#19091,#19092,#19093,#19094,#19095,#19096,#19097,#19098,#19099,
#19100,#19101,#19102,#19103,#19104,#19105,#19106,#19107,#19108,#19109,#19110,
#19111,#19112,#19113,#19114,#19115,#19116,#19117,#19118,#19119,#19120,#19121,
#19122,#19123,#19124,#19125,#19126,#19127,#19128,#19129,#19130,#19131,#19132,
#19133,#19134,#19135,#19136,#19137,#19138,#19139,#19140,#19141,#19142,#19143,
#19144,#19145,#19146,#19147,#19148,#19149,#19150,#19151,#19152,#19153,#19154,
#19155,#19156,#19157,#19158,#19159,#19160,#19161,#19162,#19163,#19164,#19165,
#19166,#19167,#19168,#19169,#19170,#19171,#19172,#19173,#19174,#19175,#19176,
#19177,#19178,#19179,#19180,#19181,#19182,#19183,#19184,#19185,#19186,#19187,
#19188,#19189,#19190,#19191,#19192,#19193,#19194,#19195,#19196,#19197,#19198,
#19199,#19200,#19201,#19202,#19203,#19204,#19205,#19206,#19207,#19208,#19209,
#19210,#19211,#19212,#19213,#19214,#19215,#19216,#19217,#19218,#19219,#19220,
#19221,#19222,#19223,#19224,#19225,#19226,#19227,#19228,#19229,#19230,#19231,
#19232,#19233,#19234,#19235,#19236,#19237,#19238,#19239,#19240,#19241,#19242,
#19243,#19244,#19245,#19246,#19247,#19248,#19249,#19250,#19251,#19252,#19253,
#19254,#19255,#19256,#19257,#19258,#19259,#19260,#19261,#19262,#19263,#19264,
#19265,#19266,#19267,#19268,#19269),.UNSPECIFIED.,.F.,.F.,(4,2,2,2,2,2,
2,2,2,2,2,2,2,2,2,2,2,2,2,2,2,2,2,2,2,2,2,2,2,2,2,2,2,2,2,2,2,2,2,2,2,2,
2,2,2,2,2,2,2,2,2,2,2,2,2,2,2,2,2,2,2,2,2,2,2,2,2,2,2,2,2,2,2,2,2,2,2,2,
2,2,2,2,2,2,2,2,2,2,2,2,2,2,2,2,2,2,2,2,2,2,2,2,2,2,2,2,2,2,2,2,2,2,2,2,
2,2,2,2,2,2,2,2,2,2,2,2,2,2,2,2,2,2,2,2,2,2,2,2,2,2,2,2,2,2,2,2,2,2,2,2,
2,2,2,2,2,2,2,2,2,2,2,2,2,2,2,2,2,2,2,4),(-3.4001166352834,-3.39564261836977,
-3.37616524052795,-3.36941798495544,-3.36485558168374,-3.3632482619308,
-3.36230636766994,-3.36129397703547,-3.35998890427821,-3.35728133684505,
-3.33961572743597,-3.33518013814448,-3.31906953623153,-3.24018730414167,
-3.22759461540252,-3.20720523332922,-3.20252512153085,-3.20140498778015,
-3.2007600499941,-3.20019896994023,-3.19949971659798,-3.19842041850966,
-3.19352924184026,-3.10060309886798,-3.06918752383647,-3.05210539664945,
-3.04598842633795,-3.04176762323625,-3.04020882849883,-3.03926768004243,
-3.0382503793547,-3.03693302321202,-3.03408848868579,-3.01314356240239,
-3.01028412262459,-2.92224963350563,-2.90323327544859,-2.88257465692825,
-2.87926081585319,-2.87826808666874,-2.87765162627742,-2.87708475354703,
-2.87634835100729,-2.87474866373784,-2.86275543003986,-2.78145337213415,
-2.74808258044113,-2.72361434716246,-2.72047353004736,-2.71800753224254,
-2.71675729891402,-2.71584290321642,-2.71487786799725,-2.71325460944369,
-2.70897871509158,-2.63976086734888,-2.60475770566463,-2.57659600239261,
-2.56484949276183,-2.55691103753076,-2.55560017821475,-2.55491385154032,
-2.55440773804194,-2.55385350876891,-2.55303866911201,-2.55064852714377,
-2.50952779864725,-2.47577205766266,-2.43138002370964,-2.40155082020723,
-2.39801897501125,-2.396115577788,-2.39447877729578,-2.39341301322893,-2.39239261644031,
-2.39105652283003,-2.388809206635,-2.3752284595319,-2.37482097768049,-2.37105931791733,
-2.36986421081892,-2.3683635813474,-2.36191857079865,-2.33260941447581,
-2.31329725759443,-2.27791843377717,-2.24938214713646,-2.23444088820955,
-2.23293162307917,-2.23220478034812,-2.23169321709032,-2.23115610611128,
-2.23040323354746,-2.22842467048224,-2.19790230589511,-2.16823799983893,
-2.11866638260439,-2.07991458848427,-2.07578462549641,-2.07268303192678,
-2.07130320632852,-2.07027946409882,-2.06932844546283,-2.06802938822681,
-2.06546306160851,-2.04434849015913,-2.04280191404333,-2.03145870303487,
-1.98649813292062,-1.91513391353612,-1.91095137650226,-1.90983316408563,
-1.90918201246127,-1.90862145705115,-1.90793037727574,-1.90659705049921,
-1.89812291193671,-1.87875205747178,-1.83287173781374,-1.7859622288385,
-1.77835402456422,-1.77209394423961,-1.77063563252481,-1.76943343616851,
-1.76774319362738,-1.76567945694773,-1.76394298951131,-1.76355309734664,
-1.7626563397301,-1.76035941487434,-1.75150420858391,-1.74951747451604,
-1.74824588494161,-1.7472372968675,-1.74610676149564,-1.74422150470573,
-1.73726668053863,-1.69079917427546,-1.60332742698091,-1.6029479463537,
-1.60067882859647,-1.59985317398128,-1.5887261823831,-1.58718007304828,
-1.58644282478939,-1.58587574275852,-1.5852719599226,-1.5843134936857,-1.58318249126872,
-1.58102415313264,-1.53260425992577,-1.45501474975192,-1.44886593969182,
-1.44755085003209,-1.44634616004722,-1.44482420145199,-1.44274506882589,
-1.44209996053122,-1.44096799817853,-1.44013234428156,-1.43846164559023,
-1.4346519845408,-1.42798591948393,-1.42604390303145,-1.42490061909869,
-1.4239033794519,-1.42265591411376,-1.42023318024337,-1.40418746964708,
-1.37062515302182),.UNSPECIFIED.);
#116=B_SPLINE_CURVE_WITH_KNOTS('',3,(#19271,#19272,#19273,#19274,#19275,
#19276,#19277,#19278,#19279,#19280,#19281,#19282,#19283,#19284,#19285,#19286,
#19287,#19288,#19289,#19290,#19291,#19292,#19293,#19294,#19295,#19296,#19297,
#19298,#19299,#19300,#19301,#19302,#19303,#19304,#19305,#19306,#19307,#19308,
#19309,#19310,#19311,#19312,#19313,#19314,#19315,#19316,#19317,#19318,#19319,
#19320,#19321,#19322,#19323,#19324,#19325,#19326,#19327,#19328,#19329,#19330,
#19331,#19332,#19333,#19334,#19335,#19336,#19337,#19338,#19339,#19340,#19341,
#19342,#19343,#19344,#19345,#19346,#19347,#19348,#19349,#19350,#19351,#19352,
#19353,#19354,#19355,#19356,#19357,#19358,#19359,#19360,#19361,#19362,#19363,
#19364,#19365,#19366,#19367,#19368,#19369,#19370,#19371,#19372,#19373,#19374,
#19375,#19376,#19377,#19378,#19379,#19380,#19381,#19382,#19383,#19384,#19385,
#19386,#19387,#19388,#19389,#19390,#19391,#19392,#19393,#19394,#19395,#19396,
#19397,#19398,#19399,#19400,#19401,#19402),.UNSPECIFIED.,.F.,.F.,(4,2,2,
2,2,2,2,2,2,2,2,2,2,2,2,2,2,2,2,2,2,2,2,2,2,2,2,2,2,2,2,2,2,2,2,2,2,2,2,
2,2,2,2,2,2,2,2,2,2,2,2,2,2,2,2,2,2,2,2,2,2,2,2,2,2,4),(-0.661909204026248,
-0.64894264803278,-0.615825256544206,-0.5443609960742,-0.516002197635334,
-0.512916278428946,-0.511676844897361,-0.510646912975357,-0.509594162221055,
-0.508063426432141,-0.504058319056844,-0.451014403122912,-0.441219446831309,
-0.433199637354459,-0.426413430898802,-0.420550549096795,-0.415409209026523,
-0.368269023539108,-0.366492418389508,-0.36602307444709,-0.364593807208228,
-0.363806897593697,-0.3519689895989,-0.350533823138102,-0.34980916580575,
-0.34927943892428,-0.348744958111922,-0.347997179095996,-0.346367121026489,
-0.344191805489356,-0.338937959916859,-0.328394755129598,-0.308502790868293,
-0.2190657860621,-0.212593682883621,-0.21109924407627,-0.209904353644704,
-0.205963735391409,-0.205409206202199,-0.203284985320601,-0.201550802131789,
-0.197675256604626,-0.191141340166538,-0.189214338808994,-0.18807444314546,
-0.187167957324008,-0.185957437854189,-0.183709052622849,-0.171608261792693,
-0.147728591862738,-0.052618070603708,-0.0489589398069684,-0.0444524664038431,
-0.0436386920629048,-0.0417526484775384,-0.0413534608729569,-0.0400173683724421,
-0.0288495962310037,-0.0273017853572611,-0.0265641664968555,-0.0259969993937612,
-0.025471908524072,-0.0248660680095603,-0.0240071157144323,-0.0225391935736945,
-0.000960648637719504),.UNSPECIFIED.);
#117=B_SPLINE_CURVE_WITH_KNOTS('',3,(#19403,#19404,#19405,#19406,#19407,
#19408,#19409,#19410,#19411,#19412,#19413,#19414,#19415,#19416,#19417,#19418,
#19419,#19420,#19421,#19422,#19423,#19424,#19425,#19426,#19427,#19428,#19429,
#19430,#19431,#19432,#19433,#19434,#19435,#19436,#19437,#19438,#19439,#19440,
#19441,#19442,#19443,#19444,#19445,#19446,#19447,#19448,#19449,#19450,#19451,
#19452,#19453,#19454,#19455,#19456,#19457,#19458,#19459,#19460,#19461,#19462,
#19463,#19464,#19465,#19466,#19467,#19468,#19469,#19470,#19471,#19472,#19473,
#19474,#19475,#19476,#19477,#19478,#19479,#19480,#19481,#19482,#19483,#19484,
#19485,#19486,#19487,#19488,#19489,#19490,#19491,#19492,#19493,#19494,#19495,
#19496,#19497,#19498,#19499,#19500,#19501,#19502,#19503,#19504,#19505,#19506,
#19507,#19508,#19509,#19510,#19511,#19512,#19513,#19514,#19515,#19516,#19517,
#19518,#19519,#19520,#19521,#19522,#19523,#19524,#19525,#19526,#19527,#19528,
#19529,#19530,#19531,#19532,#19533,#19534,#19535,#19536,#19537,#19538,#19539,
#19540,#19541,#19542,#19543,#19544,#19545,#19546,#19547,#19548,#19549,#19550,
#19551,#19552,#19553,#19554,#19555,#19556,#19557,#19558,#19559,#19560,#19561,
#19562,#19563,#19564,#19565,#19566,#19567,#19568,#19569,#19570,#19571,#19572,
#19573,#19574,#19575,#19576,#19577,#19578,#19579,#19580,#19581,#19582,#19583,
#19584,#19585,#19586,#19587,#19588,#19589,#19590,#19591,#19592,#19593,#19594,
#19595,#19596,#19597,#19598,#19599,#19600,#19601,#19602,#19603,#19604,#19605,
#19606,#19607,#19608,#19609,#19610,#19611,#19612,#19613,#19614,#19615,#19616,
#19617,#19618,#19619,#19620,#19621,#19622,#19623,#19624,#19625,#19626,#19627,
#19628,#19629,#19630,#19631,#19632,#19633,#19634,#19635,#19636,#19637,#19638,
#19639,#19640,#19641,#19642,#19643,#19644,#19645,#19646,#19647,#19648),
 .UNSPECIFIED.,.F.,.F.,(4,2,2,2,2,2,2,2,2,2,2,2,2,2,2,2,2,2,2,2,2,2,2,2,
2,2,2,2,2,2,2,2,2,2,2,2,2,2,2,2,2,2,2,2,2,2,2,2,2,2,2,2,2,2,2,2,2,2,2,2,
2,2,2,2,2,2,2,2,2,2,2,2,2,2,2,2,2,2,2,2,2,2,2,2,2,2,2,2,2,2,2,2,2,2,2,2,
2,2,2,2,2,2,2,2,2,2,2,2,2,2,2,2,2,2,2,2,2,2,2,2,2,2,4),(-4.06067477183731,
-3.97551640619293,-3.9342284616751,-3.92772495826773,-3.92588498946432,
-3.92476517266495,-3.92375554426393,-3.92246814951183,-3.91984686563877,
-3.90396583415625,-3.90295869860179,-3.90173117253988,-3.9002119804425,
-3.89432030234605,-3.81658839468245,-3.79159166232957,-3.77368860319943,
-3.7682250166568,-3.76598654563151,-3.76432118432354,-3.76356574784999,
-3.76303343468061,-3.76250682440761,-3.76179313429406,-3.76039961735992,
-3.74968903149156,-3.71625838004261,-3.69518018081669,-3.65201766648963,
-3.62047670404653,-3.60604092805952,-3.60368353731701,-3.60245037507324,
-3.60144569757689,-3.60029045863565,-3.59834286996244,-3.59140702241851,
-3.58774543555818,-3.58406071244966,-3.58305700211639,-3.57976601426175,
-3.57857133878931,-3.57704299950396,-3.57063533556551,-3.49353204733034,
-3.4686513064837,-3.45331140846403,-3.45076992011312,-3.44549699742683,
-3.44331638907036,-3.44217719964726,-3.44121278003219,-3.44060813199362,
-3.44004195136439,-3.43930817802696,-3.4377209417783,-3.42603375358544,
-3.42513867933139,-3.42458461240024,-3.4237335467686,-3.4233510596538,-3.42250904713076,
-3.42040822392064,-3.41894690111654,-3.37564523076464,-3.33228234050492,
-3.30279574465384,-3.28367426668513,-3.28115146415914,-3.27988389619273,
-3.27897112507605,-3.27800382166548,-3.2766419577825,-3.27382280010805,
-3.26624431667473,-3.26443066446623,-3.26236874195894,-3.26192149977942,
-3.26002087266932,-3.25718406517421,-3.25453080176283,-3.24819757365304,
-3.15838578792251,-3.13280354848664,-3.12441487666233,-3.12134610741856,
-3.11988342403432,-3.11870176475175,-3.1180820179147,-3.1175329884998,-3.11688018000654,
-3.11575395648471,-3.11148714487279,-3.10871771107924,-3.10720408449865,
-3.10598422312306,-3.08739565940028,-2.99793681821398,-2.97315817473116,
-2.96044088479583,-2.95816211305024,-2.956945569,-2.95594167196336,-2.95492555898799,
-2.95304510364951,-2.94690220825838,-2.83798881269394,-2.82054046335701,
-2.79987321065769,-2.79767658182068,-2.79653124418734,-2.79556254638864,
-2.79495682144533,-2.79439079408035,-2.79365880230651,-2.79208153670383,
-2.78065897366069,-2.77954596476192,-2.777999644062,-2.77492103113334,-2.75066375205298,
-2.7183576420267,-2.6926898927874),.UNSPECIFIED.);
#118=B_SPLINE_CURVE_WITH_KNOTS('',3,(#19654,#19655,#19656,#19657,#19658,
#19659,#19660,#19661,#19662,#19663,#19664,#19665,#19666,#19667,#19668,#19669,
#19670,#19671,#19672,#19673,#19674,#19675,#19676,#19677,#19678,#19679,#19680,
#19681,#19682,#19683,#19684,#19685,#19686,#19687,#19688,#19689,#19690,#19691,
#19692,#19693,#19694,#19695,#19696,#19697,#19698,#19699,#19700,#19701,#19702,
#19703,#19704,#19705,#19706,#19707,#19708,#19709,#19710,#19711,#19712,#19713,
#19714,#19715,#19716,#19717,#19718,#19719,#19720,#19721,#19722,#19723,#19724,
#19725,#19726,#19727,#19728,#19729,#19730,#19731,#19732,#19733,#19734,#19735,
#19736,#19737,#19738,#19739,#19740,#19741,#19742,#19743,#19744,#19745,#19746,
#19747,#19748,#19749,#19750,#19751,#19752,#19753,#19754,#19755,#19756,#19757,
#19758,#19759,#19760,#19761,#19762,#19763,#19764,#19765,#19766,#19767,#19768,
#19769,#19770,#19771,#19772,#19773,#19774,#19775,#19776,#19777,#19778,#19779,
#19780,#19781,#19782,#19783,#19784,#19785,#19786,#19787,#19788,#19789,#19790,
#19791,#19792,#19793,#19794,#19795,#19796,#19797,#19798,#19799,#19800,#19801,
#19802,#19803,#19804,#19805,#19806,#19807,#19808,#19809,#19810,#19811,#19812,
#19813,#19814,#19815,#19816,#19817,#19818,#19819,#19820,#19821,#19822,#19823,
#19824,#19825,#19826,#19827,#19828,#19829,#19830,#19831,#19832,#19833,#19834,
#19835,#19836,#19837,#19838,#19839,#19840,#19841,#19842,#19843,#19844,#19845,
#19846,#19847,#19848,#19849),.UNSPECIFIED.,.F.,.F.,(4,2,2,2,2,2,2,2,2,2,
2,2,2,2,2,2,2,2,2,2,2,2,2,2,2,2,2,2,2,2,2,2,2,2,2,2,2,2,2,2,2,2,2,2,2,2,
2,2,2,2,2,2,2,2,2,2,2,2,2,2,2,2,2,2,2,2,2,2,2,2,2,2,2,2,2,2,2,2,2,2,2,2,
2,2,2,2,2,2,2,2,2,2,2,2,2,2,2,4),(-1.36960102657385,-1.34982761332196,-1.24890809839695,
-1.24272075299376,-1.24083457604496,-1.23981708968323,-1.23882252599685,
-1.2376358992272,-1.23547225687161,-1.23279091301979,-1.18122375085026,
-1.08474811374041,-1.07991196085698,-1.0788371021054,-1.07813924133682,
-1.07757827990661,-1.07693236305532,-1.0758077688474,-1.07107060341839,
-1.02886732836974,-0.946595968867606,-0.940605099092659,-0.939049465645938,
-0.937816098240649,-0.936810060770758,-0.92096351145887,-0.918342767296007,
-0.91705498295753,-0.916044747584459,-0.914946559303704,-0.913164350388299,
-0.907173809342364,-0.89762015760281,-0.865676629489227,-0.826471418902932,
-0.760631984890354,-0.756821620927213,-0.75572952277531,-0.755154617222093,
-0.75465069049022,-0.753996807615432,-0.752836133365388,-0.747612150863471,
-0.689411339787425,-0.633110379915867,-0.620751973431156,-0.617906243109689,
-0.616480196360992,-0.615273714997185,-0.613866172069521,-0.61176986249144,
-0.611258779020742,-0.608228095142774,-0.605285835283282,-0.601712844553965,
-0.599768078656407,-0.596092818235156,-0.594722176292371,-0.593752172237995,
-0.592839706060771,-0.591867511500152,-0.589828663436281,-0.580990681173594,
-0.565079977637646,-0.526060554051278,-0.438872147529599,-0.434072173214614,
-0.433000184184496,-0.432303181670121,-0.431742232340601,-0.431095571433228,
-0.429967797566877,-0.425190683234534,-0.370339811654537,-0.346775348786968,
-0.317096885436763,-0.301345038953997,-0.295090898114237,-0.291384491907739,
-0.275222402886052,-0.272585379971146,-0.271294188797298,-0.270283386382439,
-0.269340702951088,-0.268243023454457,-0.265030388520121,-0.233332259594882,
-0.21335180609637,-0.115854043978622,-0.111506568750345,-0.110078756724497,
-0.109358220791414,-0.108794973226389,-0.108163552433763,-0.107104517788285,
-0.103138472583711,-0.0751682503225802,-0.000962417701089617),
 .UNSPECIFIED.);
#119=B_SPLINE_CURVE_WITH_KNOTS('',3,(#19850,#19851,#19852,#19853,#19854,
#19855,#19856,#19857,#19858,#19859,#19860,#19861,#19862,#19863,#19864,#19865,
#19866,#19867,#19868,#19869,#19870,#19871,#19872,#19873,#19874,#19875,#19876,
#19877,#19878,#19879,#19880,#19881,#19882,#19883,#19884,#19885,#19886,#19887,
#19888,#19889,#19890,#19891,#19892,#19893,#19894,#19895,#19896,#19897,#19898,
#19899,#19900,#19901,#19902,#19903,#19904,#19905,#19906,#19907,#19908,#19909,
#19910,#19911,#19912,#19913,#19914,#19915,#19916,#19917,#19918,#19919,#19920,
#19921,#19922,#19923,#19924,#19925,#19926,#19927,#19928,#19929,#19930,#19931,
#19932,#19933,#19934,#19935,#19936,#19937,#19938,#19939,#19940,#19941,#19942,
#19943),.UNSPECIFIED.,.F.,.F.,(4,2,2,2,2,2,2,2,2,2,2,2,2,2,2,2,2,2,2,2,
2,2,2,2,2,2,2,2,2,2,2,2,2,2,2,2,2,2,2,2,2,2,2,2,2,2,4),(-4.06128526371725,
-4.01403618995952,-4.01152595456631,-4.01003311647368,-4.00896502788193,
-4.00802392688564,-4.00700442585582,-4.00567317438803,-4.00286152966641,
-3.98182348253844,-3.97954915416361,-3.96368781931084,-3.95863231897075,
-3.95274423953934,-3.87253627244141,-3.85144434700357,-3.84808841602249,
-3.84709110228388,-3.84647363530591,-3.84590712421589,-3.84517295092564,
-3.84358495971133,-3.83189569354908,-3.83099593072355,-3.75034058225151,
-3.73224143377886,-3.70305082147155,-3.68908120855673,-3.68675054332559,
-3.68574863716805,-3.68472746022651,-3.68377252179041,-3.68245826359875,
-3.67912746588137,-3.63618255982295,-3.58765059069244,-3.58169623636757,
-3.52890990782499,-3.52526005340221,-3.52423192291307,-3.52360755959704,
-3.52304300081289,-3.52232243367425,-3.52080540484074,-3.51081153605494,
-3.43568210163337,-3.4001166352834),.UNSPECIFIED.);
#120=B_SPLINE_CURVE_WITH_KNOTS('',3,(#19944,#19945,#19946,#19947,#19948,
#19949,#19950,#19951,#19952,#19953,#19954,#19955,#19956,#19957,#19958,#19959,
#19960,#19961,#19962,#19963,#19964,#19965,#19966,#19967,#19968,#19969,#19970,
#19971,#19972,#19973,#19974,#19975,#19976,#19977,#19978,#19979,#19980,#19981,
#19982,#19983,#19984,#19985,#19986,#19987,#19988,#19989,#19990,#19991,#19992,
#19993,#19994,#19995,#19996,#19997,#19998,#19999,#20000,#20001,#20002,#20003,
#20004,#20005,#20006,#20007,#20008,#20009,#20010,#20011,#20012,#20013,#20014,
#20015,#20016,#20017,#20018,#20019,#20020,#20021,#20022,#20023,#20024,#20025,
#20026,#20027,#20028,#20029,#20030,#20031,#20032,#20033,#20034,#20035,#20036,
#20037,#20038,#20039,#20040,#20041,#20042,#20043,#20044,#20045,#20046,#20047,
#20048,#20049,#20050,#20051,#20052,#20053,#20054,#20055,#20056,#20057,#20058,
#20059,#20060,#20061,#20062,#20063,#20064,#20065,#20066,#20067,#20068,#20069,
#20070,#20071,#20072,#20073,#20074,#20075,#20076,#20077,#20078,#20079,#20080,
#20081,#20082,#20083,#20084,#20085,#20086,#20087,#20088,#20089,#20090,#20091,
#20092,#20093,#20094,#20095,#20096,#20097,#20098,#20099,#20100,#20101,#20102,
#20103,#20104,#20105,#20106,#20107,#20108,#20109,#20110,#20111,#20112,#20113,
#20114,#20115,#20116,#20117,#20118,#20119,#20120,#20121,#20122,#20123,#20124,
#20125,#20126,#20127,#20128,#20129,#20130,#20131,#20132,#20133,#20134,#20135,
#20136,#20137,#20138,#20139,#20140,#20141,#20142,#20143,#20144,#20145,#20146,
#20147,#20148,#20149,#20150,#20151,#20152,#20153,#20154,#20155,#20156,#20157,
#20158,#20159,#20160,#20161,#20162,#20163,#20164,#20165,#20166,#20167,#20168,
#20169,#20170,#20171,#20172,#20173,#20174,#20175,#20176,#20177,#20178,#20179,
#20180,#20181,#20182,#20183,#20184,#20185,#20186,#20187,#20188,#20189,#20190,
#20191,#20192,#20193,#20194,#20195,#20196,#20197,#20198,#20199,#20200,#20201,
#20202,#20203,#20204,#20205,#20206,#20207,#20208,#20209,#20210,#20211,#20212,
#20213,#20214,#20215),.UNSPECIFIED.,.F.,.F.,(4,2,2,2,2,2,2,2,2,2,2,2,2,
2,2,2,2,2,2,2,2,2,2,2,2,2,2,2,2,2,2,2,2,2,2,2,2,2,2,2,2,2,2,2,2,2,2,2,2,
2,2,2,2,2,2,2,2,2,2,2,2,2,2,2,2,2,2,2,2,2,2,2,2,2,2,2,2,2,2,2,2,2,2,2,2,
2,2,2,2,2,2,2,2,2,2,2,2,2,2,2,2,2,2,2,2,2,2,2,2,2,2,2,2,2,2,2,2,2,2,2,2,
2,2,2,2,2,2,2,2,2,2,2,2,2,2,4),(-2.6926898927874,-2.67309610584487,-2.65079332468313,
-2.6376223350769,-2.63532116467435,-2.63409967375698,-2.63309533864024,
-2.632081881767,-2.63021533282697,-2.6241895089379,-2.50797674714693,-2.4903136656093,
-2.47608552821513,-2.4743172710447,-2.47333762249951,-2.47268205537713,
-2.47207555368219,-2.4715271305527,-2.47082739347038,-2.46974645239456,
-2.46483403008942,-2.36982806351589,-2.3520224639032,-2.32724270077514,
-2.31445625380223,-2.31217338982096,-2.31095567275187,-2.30995133689594,
-2.30893523174088,-2.30705610907138,-2.30092818926197,-2.19266536184236,
-2.15174924909108,-2.15000257646364,-2.14923082951768,-2.14866036331882,
-2.14812664817978,-2.14738657584853,-2.14589004330382,-2.13213786646308,
-2.13030845937606,-2.03150354455633,-2.01578039377114,-2.01323778502252,
-1.99220920365282,-1.9893978529876,-1.98806664174814,-1.98704712776963,
-1.98595762336159,-1.98425556599443,-1.97899618841049,-1.94972598638336,
-1.90580790895638,-1.83203006109701,-1.82778063464633,-1.82665580497947,
-1.82600314062181,-1.82544273263893,-1.82475365742679,-1.82342974653971,
-1.81518440728078,-1.79747160871322,-1.77256181535091,-1.70505671542748,
-1.66994256903903,-1.66675631053237,-1.665466817991,-1.66451827091473,-1.66351352612049,
-1.66216680657377,-1.66067109200021,-1.65815396504563,-1.59784210417049,
-1.50966089918513,-1.50862858552766,-1.50475311233365,-1.50366667055202,
-1.50302290574208,-1.50246162346838,-1.5017605388016,-1.50037923993155,
-1.49059743568069,-1.46602356718208,-1.35040889565067,-1.34445907007786,
-1.34260159083249,-1.34158982239805,-1.34058510790954,-1.33938500790588,
-1.33715211052937,-1.33437093403008,-1.28554542521502,-1.19180671739098,
-1.19006458328631,-1.1888837108712,-1.1820399564423,-1.18079197504582,-1.18004941480431,
-1.1794815650415,-1.17886788367999,-1.17788763418365,-1.17468537838819,
-1.12650129169932,-1.03420952760566,-1.03353359906517,-1.03070056822006,
-1.02193126400388,-1.01999500356996,-1.01873916102006,-1.01773219189751,
-1.01661487386807,-1.01475541697356,-1.01252870448309,-1.00814894137876,
-0.997248604953662,-0.957641827754534,-0.863436897465518,-0.858642230018257,
-0.857570621662452,-0.856873719572898,-0.856312751700649,-0.855665957665397,
-0.854537673064802,-0.849754446542577,-0.794918901056801,-0.727925121726972,
-0.700390097395911,-0.697633517928579,-0.696286600793523,-0.695322911328846,
-0.694352622595137,-0.693069516366336,-0.690446835669292,-0.687057802964749,
-0.679334366621671,-0.662311037573458),.UNSPECIFIED.);
#121=B_SPLINE_CURVE_WITH_KNOTS('',3,(#20220,#20221,#20222,#20223,#20224,
#20225,#20226,#20227,#20228,#20229,#20230,#20231,#20232,#20233,#20234,#20235,
#20236,#20237,#20238,#20239,#20240,#20241,#20242,#20243,#20244,#20245,#20246,
#20247,#20248,#20249,#20250,#20251,#20252,#20253,#20254,#20255,#20256,#20257,
#20258,#20259,#20260,#20261,#20262,#20263,#20264,#20265,#20266,#20267,#20268,
#20269,#20270,#20271,#20272,#20273,#20274,#20275,#20276,#20277,#20278,#20279,
#20280,#20281,#20282,#20283,#20284,#20285,#20286,#20287,#20288,#20289,#20290,
#20291,#20292,#20293,#20294,#20295,#20296,#20297,#20298,#20299,#20300,#20301,
#20302,#20303,#20304,#20305,#20306,#20307,#20308,#20309,#20310,#20311,#20312,
#20313,#20314,#20315,#20316,#20317,#20318,#20319,#20320,#20321,#20322,#20323,
#20324,#20325,#20326,#20327,#20328,#20329,#20330,#20331,#20332,#20333,#20334,
#20335,#20336,#20337,#20338,#20339,#20340,#20341,#20342,#20343,#20344,#20345,
#20346,#20347,#20348,#20349,#20350,#20351,#20352,#20353,#20354,#20355,#20356,
#20357,#20358,#20359,#20360,#20361,#20362,#20363,#20364,#20365,#20366,#20367,
#20368,#20369,#20370,#20371,#20372,#20373,#20374,#20375,#20376,#20377,#20378,
#20379,#20380,#20381,#20382,#20383,#20384,#20385,#20386,#20387,#20388,#20389,
#20390,#20391,#20392,#20393,#20394,#20395,#20396,#20397,#20398,#20399,#20400,
#20401,#20402,#20403,#20404,#20405,#20406,#20407,#20408,#20409,#20410,#20411,
#20412,#20413,#20414,#20415,#20416,#20417,#20418,#20419,#20420,#20421,#20422,
#20423,#20424,#20425,#20426,#20427,#20428,#20429,#20430,#20431,#20432,#20433,
#20434,#20435,#20436,#20437,#20438,#20439,#20440,#20441,#20442,#20443,#20444,
#20445,#20446,#20447,#20448,#20449,#20450,#20451,#20452,#20453,#20454,#20455,
#20456,#20457,#20458,#20459,#20460,#20461,#20462,#20463,#20464,#20465,#20466,
#20467,#20468,#20469,#20470,#20471,#20472,#20473,#20474,#20475,#20476,#20477,
#20478,#20479,#20480,#20481,#20482,#20483,#20484,#20485,#20486,#20487,#20488,
#20489,#20490,#20491,#20492,#20493,#20494,#20495,#20496,#20497,#20498,#20499,
#20500,#20501,#20502,#20503),.UNSPECIFIED.,.F.,.F.,(4,2,2,2,2,2,2,2,2,2,
2,2,2,2,2,2,2,2,2,2,2,2,2,2,2,2,2,2,2,2,2,2,2,2,2,2,2,2,2,2,2,2,2,2,2,2,
2,2,2,2,2,2,2,2,2,2,2,2,2,2,2,2,2,2,2,2,2,2,2,2,2,2,2,2,2,2,2,2,2,2,2,2,
2,2,2,2,2,2,2,2,2,2,2,2,2,2,2,2,2,2,2,2,2,2,2,2,2,2,2,2,2,2,2,2,2,2,2,2,
2,2,2,2,2,2,2,2,2,2,2,2,2,2,2,2,2,2,2,2,2,2,2,4),(-3.39850283521087,-3.37886812956445,
-3.35863417788478,-3.34815667885647,-3.3428698297973,-3.3395876243599,-3.33885124461285,
-3.33816229195313,-3.33760213256738,-3.3370352286123,-3.33598213307277,
-3.33251025005807,-3.27716760410847,-3.22895465939362,-3.19561684758958,
-3.18075950080207,-3.17839837805032,-3.1771508565237,-3.17624071684908,
-3.17526504871281,-3.17387280024893,-3.17005745442605,-3.11028981764791,
-3.04921563593415,-3.02668723895948,-3.01751398340293,-3.01615870372652,
-3.01545749525619,-3.01494982493158,-3.01440311675706,-3.01345038785351,
-3.01074596600773,-2.96837921632043,-2.91277159198561,-2.8743181558504,
-2.8581111532748,-2.85572669639301,-2.85445870946526,-2.85354576295307,
-2.85257839079847,-2.85121662197714,-2.84839828479699,-2.84081673236981,
-2.83900228001641,-2.8369399274836,-2.83649857993593,-2.83454470737958,
-2.83176097806481,-2.82864398242382,-2.76037986710993,-2.72113089851205,
-2.69774691342335,-2.69538517933984,-2.69364243940109,-2.69286518531221,
-2.69229398386132,-2.69176206386797,-2.69102820915135,-2.68916360644994,
-2.66571984327507,-2.59663181379918,-2.54019963759614,-2.53622532688605,
-2.53324123818374,-2.53187052946614,-2.53084866246442,-2.52989586798446,
-2.52858891470685,-2.52599041901296,-2.50388608054255,-2.49189420206403,
-2.40209123729086,-2.38080309629431,-2.37192935284491,-2.37058498347194,
-2.36988602781303,-2.36932513602276,-2.36876374324739,-2.36773823531028,
-2.36449315455294,-2.32356634328817,-2.30068727261435,-2.25214754331056,
-2.21396008915135,-2.21058521867599,-2.20915720567671,-2.20812512394539,
-2.20718529483922,-2.20592988903343,-2.2028710916244,-2.17397654566229,
-2.10376167784597,-2.05161848634036,-2.04846670436279,-2.04749241938952,
-2.04688018907063,-2.04631204496277,-2.04556682040451,-2.04398010615256,
-2.03177749085631,-2.03070064005706,-2.00584359882914,-1.91841591852406,
-1.89063640474908,-1.88756777891063,-1.88633158265758,-1.88530287138216,
-1.88424986712639,-1.88271602355577,-1.87868731257916,-1.82427536413008,
-1.73814774423759,-1.72657719722811,-1.72515173125588,-1.72442968233519,
-1.72390076138609,-1.72332719049738,-1.72253704007209,-1.7206861526361,
-1.66815061273637,-1.59809180037001,-1.56782790453629,-1.56500562514299,
-1.56364274645502,-1.56267494712003,-1.56176189117269,-1.56051969634375,
-1.55809103037091,-1.55500826702422,-1.53130386529167,-1.50867529136043,
-1.41839328011026,-1.41712017264588,-1.41530234542897,-1.40366426115492,
-1.4022363065904,-1.40151358132533,-1.40098444574681,-1.40041092582284,
-1.39962133865539,-1.39777399412751,-1.36960102657385),.UNSPECIFIED.);
#122=B_SPLINE_CURVE_WITH_KNOTS('',3,(#20505,#20506,#20507,#20508,#20509,
#20510,#20511,#20512,#20513,#20514,#20515,#20516,#20517,#20518,#20519,#20520,
#20521,#20522,#20523,#20524,#20525,#20526,#20527,#20528,#20529,#20530,#20531,
#20532,#20533,#20534,#20535,#20536,#20537,#20538,#20539,#20540,#20541,#20542,
#20543,#20544,#20545,#20546,#20547,#20548,#20549,#20550,#20551,#20552,#20553,
#20554,#20555,#20556,#20557,#20558,#20559,#20560,#20561,#20562,#20563,#20564,
#20565,#20566,#20567,#20568,#20569,#20570,#20571,#20572,#20573,#20574,#20575,
#20576,#20577,#20578,#20579,#20580,#20581,#20582,#20583,#20584,#20585,#20586,
#20587,#20588,#20589,#20590,#20591,#20592,#20593,#20594,#20595,#20596,#20597,
#20598,#20599,#20600,#20601,#20602,#20603,#20604,#20605,#20606,#20607,#20608,
#20609,#20610,#20611,#20612,#20613,#20614,#20615,#20616,#20617,#20618,#20619,
#20620),.UNSPECIFIED.,.F.,.F.,(4,2,2,2,2,2,2,2,2,2,2,2,2,2,2,2,2,2,2,2,
2,2,2,2,2,2,2,2,2,2,2,2,2,2,2,2,2,2,2,2,2,2,2,2,2,2,2,2,2,2,2,2,2,2,2,2,
2,4),(-0.662311037573458,-0.65615864758013,-0.621327529538634,-0.546607691738824,
-0.536271025882487,-0.534891182292375,-0.53418071286439,-0.533654619493689,
-0.533078302530182,-0.532274100277144,-0.530342446873173,-0.527677247150757,
-0.498714599855855,-0.473433228537379,-0.467231993997839,-0.461833297893715,
-0.414695956770623,-0.403065358324979,-0.396789851754358,-0.377110831010752,
-0.374595601363168,-0.373309493263339,-0.372361668917608,-0.371401948437605,
-0.370403468112348,-0.36810717373799,-0.354906680588511,-0.333674848406216,
-0.312504400846729,-0.217671366150407,-0.21275570861585,-0.211674206174472,
-0.210974135129431,-0.210412807011706,-0.209768036166981,-0.208649307564375,
-0.203990371876987,-0.181168749103709,-0.0987139729391346,-0.0929458877557674,
-0.0867890769430741,-0.0761086949448165,-0.0716907483743516,-0.0704319797769508,
-0.069289570689577,-0.0672269001869602,-0.0645928228927022,-0.0622057754009242,
-0.0552355304567586,-0.0516840728705253,-0.0503329443696014,-0.0493679951394072,
-0.0483967711885841,-0.0474118047662053,-0.0461420102717969,-0.0441651812178458,
-0.0418034854322739,-0.000960728331950941),.UNSPECIFIED.);
#123=B_SPLINE_CURVE_WITH_KNOTS('',3,(#20621,#20622,#20623,#20624,#20625,
#20626,#20627,#20628,#20629,#20630,#20631,#20632,#20633,#20634,#20635,#20636,
#20637,#20638,#20639,#20640,#20641,#20642,#20643,#20644,#20645,#20646,#20647,
#20648,#20649,#20650,#20651,#20652,#20653,#20654,#20655,#20656,#20657,#20658,
#20659,#20660,#20661,#20662,#20663,#20664,#20665,#20666,#20667,#20668,#20669,
#20670,#20671,#20672,#20673,#20674,#20675,#20676,#20677,#20678,#20679,#20680,
#20681,#20682,#20683,#20684,#20685,#20686,#20687,#20688,#20689,#20690,#20691,
#20692,#20693,#20694,#20695,#20696,#20697,#20698,#20699,#20700,#20701,#20702,
#20703,#20704,#20705,#20706,#20707,#20708,#20709,#20710,#20711,#20712,#20713,
#20714,#20715,#20716,#20717,#20718,#20719,#20720,#20721,#20722,#20723,#20724,
#20725,#20726,#20727,#20728,#20729,#20730,#20731,#20732,#20733,#20734,#20735,
#20736,#20737,#20738,#20739,#20740,#20741,#20742,#20743,#20744,#20745,#20746,
#20747,#20748,#20749,#20750,#20751,#20752,#20753,#20754,#20755,#20756,#20757,
#20758,#20759,#20760,#20761,#20762,#20763,#20764,#20765,#20766,#20767,#20768,
#20769,#20770,#20771,#20772,#20773,#20774,#20775,#20776,#20777,#20778,#20779,
#20780,#20781,#20782,#20783,#20784,#20785,#20786,#20787,#20788,#20789,#20790,
#20791,#20792,#20793,#20794,#20795,#20796,#20797,#20798,#20799,#20800,#20801,
#20802,#20803,#20804,#20805,#20806,#20807,#20808,#20809,#20810,#20811,#20812,
#20813,#20814,#20815,#20816,#20817,#20818,#20819,#20820,#20821,#20822,#20823,
#20824,#20825,#20826,#20827,#20828,#20829,#20830,#20831,#20832),
 .UNSPECIFIED.,.F.,.F.,(4,2,2,2,2,2,2,2,2,2,2,2,2,2,2,2,2,2,2,2,2,2,2,2,
2,2,2,2,2,2,2,2,2,2,2,2,2,2,2,2,2,2,2,2,2,2,2,2,2,2,2,2,2,2,2,2,2,2,2,2,
2,2,2,2,2,2,2,2,2,2,2,2,2,2,2,2,2,2,2,2,2,2,2,2,2,2,2,2,2,2,2,2,2,2,2,2,
2,2,2,2,2,2,2,2,2,4),(-4.06063332408298,-3.98236991709419,-3.95320453615512,
-3.95052955335759,-3.94859227911098,-3.94778707522546,-3.94721052505372,
-3.94668456591702,-3.94597477485033,-3.94459770260344,-3.93433364574729,
-3.84157460790404,-3.82739425556801,-3.80261686092121,-3.78982620747972,
-3.78754935282277,-3.78655292974462,-3.78559181464287,-3.78464181428129,
-3.78334716467498,-3.7801320560732,-3.74366656763003,-3.70375877370762,
-3.67040461009186,-3.64521482460296,-3.63271241003713,-3.62646192791595,
-3.62523558672442,-3.62456727221709,-3.6240626119361,-3.62341321174684,
-3.62230269576563,-3.6181969932488,-3.61785402268241,-3.61743362918342,
-3.52933667216842,-3.49468886115026,-3.4764059325892,-3.46997087970417,
-3.467011779248,-3.4646678291807,-3.46344063939049,-3.46244924477717,-3.46131146910951,
-3.45939393506891,-3.45294245443382,-3.44902628257763,-3.44725068513935,
-3.44510421343851,-3.4430214198239,-3.44121546447319,-3.43999371677761,
-3.43576387757898,-3.38331862852359,-3.3478774847442,-3.31901016227127,
-3.30881699017053,-3.30343285852135,-3.30226097034257,-3.30160456531029,
-3.30110050550384,-3.30052738456975,-3.29944441106512,-3.2957169802745,
-3.29486140579635,-3.21946970695645,-3.17112487026757,-3.1533080760608,
-3.14699593738473,-3.14407893408819,-3.14175845196327,-3.14053847068118,
-3.13954367627796,-3.13854584456083,-3.13675808601833,-3.13135286050662,
-3.126606525182,-3.12502934150732,-3.12400333337963,-3.12353258683031,-3.12233498535378,
-3.1202435137834,-3.11634149039697,-3.11276022528805,-3.01163211448398,
-2.98972837020966,-2.98069498812585,-2.97933988969156,-2.9786441827773,
-2.97808323518364,-2.97751952974331,-2.97648355902078,-2.97315703750576,
-2.91749739474139,-2.86347692809833,-2.82467482328823,-2.82140468273544,
-2.81885849671408,-2.81759011837506,-2.81661497617751,-2.81564436746798,
-2.81399355244866,-2.80954311589934,-2.73750778148851,-2.73165942825708,
-2.69197257292336),.UNSPECIFIED.);
#124=B_SPLINE_CURVE_WITH_KNOTS('',3,(#20838,#20839,#20840,#20841,#20842,
#20843,#20844,#20845,#20846,#20847,#20848,#20849,#20850,#20851,#20852,#20853,
#20854,#20855,#20856,#20857,#20858,#20859,#20860,#20861,#20862,#20863,#20864,
#20865,#20866,#20867,#20868,#20869,#20870,#20871,#20872,#20873,#20874,#20875,
#20876,#20877,#20878,#20879,#20880,#20881,#20882,#20883,#20884,#20885,#20886,
#20887,#20888,#20889,#20890,#20891,#20892,#20893,#20894,#20895,#20896,#20897,
#20898,#20899,#20900,#20901,#20902,#20903,#20904,#20905,#20906,#20907,#20908,
#20909,#20910,#20911,#20912,#20913,#20914,#20915,#20916,#20917,#20918,#20919,
#20920,#20921,#20922,#20923,#20924,#20925,#20926,#20927,#20928,#20929,#20930,
#20931,#20932,#20933,#20934,#20935,#20936,#20937,#20938,#20939,#20940,#20941,
#20942,#20943,#20944,#20945,#20946,#20947,#20948,#20949,#20950,#20951,#20952,
#20953,#20954,#20955,#20956,#20957,#20958,#20959,#20960,#20961,#20962,#20963,
#20964,#20965,#20966,#20967,#20968,#20969,#20970,#20971,#20972,#20973,#20974,
#20975,#20976,#20977,#20978,#20979,#20980,#20981,#20982,#20983,#20984,#20985,
#20986,#20987,#20988,#20989,#20990,#20991,#20992,#20993,#20994,#20995,#20996,
#20997,#20998,#20999,#21000,#21001,#21002,#21003,#21004,#21005,#21006,#21007,
#21008,#21009,#21010,#21011,#21012,#21013,#21014,#21015,#21016,#21017,#21018,
#21019,#21020,#21021),.UNSPECIFIED.,.F.,.F.,(4,2,2,2,2,2,2,2,2,2,2,2,2,
2,2,2,2,2,2,2,2,2,2,2,2,2,2,2,2,2,2,2,2,2,2,2,2,2,2,2,2,2,2,2,2,2,2,2,2,
2,2,2,2,2,2,2,2,2,2,2,2,2,2,2,2,2,2,2,2,2,2,2,2,2,2,2,2,2,2,2,2,2,2,2,2,
2,2,2,2,2,2,4),(-1.3699358201607,-1.36179106215317,-1.33700599593838,-1.26250800794385,
-1.22119362735239,-1.21873461434529,-1.21781859495292,-1.21727897556568,
-1.2167684148196,-1.21604836910061,-1.21460325264151,-1.20387418969816,
-1.1745527156667,-1.11414316664539,-1.06168371488393,-1.05822984159744,
-1.05689488358093,-1.0559343769297,-1.05491601390065,-1.05357004652269,
-1.05072962867412,-1.02626798798076,-1.01711969656458,-0.951238458716924,
-0.905843311234644,-0.905155783260641,-0.896754164277783,-0.89533322147786,
-0.894614214596374,-0.894051207980658,-0.893419040152832,-0.89276244664608,
-0.890510383945906,-0.871438213757604,-0.852249316263751,-0.803495795394027,
-0.739442413547856,-0.735500614661386,-0.734088646566974,-0.733107179052976,
-0.732197914129689,-0.730961202072346,-0.729643479836477,-0.723781333455508,
-0.714489497572144,-0.6843874755459,-0.635848988356629,-0.576781444265308,
-0.573196265074093,-0.57212946056436,-0.571559566551961,-0.571004622957775,
-0.570321975310099,-0.569594523395977,-0.566443918806259,-0.537851381464733,
-0.490782728245281,-0.417331891131705,-0.412768252981907,-0.411100235969678,
-0.410126302354737,-0.409214909514243,-0.407961207719627,-0.406619963347496,
-0.400402331781344,-0.390376348937076,-0.35566722600915,-0.319610410938011,
-0.254029909536792,-0.250280406441938,-0.249194910144441,-0.248621253097742,
-0.24811717128004,-0.247461360125111,-0.24677140022959,-0.245709852847748,
-0.232056823450463,-0.19815637288566,-0.185123259500274,-0.171506873114694,
-0.119528406112877,-0.110777651274884,-0.107669823985291,-0.0916032390522574,
-0.0889709189572523,-0.0876806029094163,-0.0866698307376031,-0.0855499228265693,
-0.0843957491233048,-0.0826936213980666,-0.0796703625964687,-0.000961575125209731),
 .UNSPECIFIED.);
#125=B_SPLINE_CURVE_WITH_KNOTS('',3,(#21022,#21023,#21024,#21025,#21026,
#21027,#21028,#21029,#21030,#21031,#21032,#21033,#21034,#21035,#21036,#21037,
#21038,#21039,#21040,#21041,#21042,#21043,#21044,#21045,#21046,#21047,#21048,
#21049,#21050,#21051,#21052,#21053,#21054,#21055,#21056,#21057,#21058,#21059,
#21060,#21061,#21062,#21063,#21064,#21065,#21066,#21067,#21068,#21069,#21070,
#21071,#21072,#21073,#21074,#21075,#21076,#21077,#21078,#21079,#21080,#21081,
#21082,#21083,#21084,#21085,#21086,#21087,#21088,#21089,#21090,#21091,#21092,
#21093,#21094,#21095,#21096,#21097,#21098,#21099,#21100,#21101,#21102,#21103,
#21104,#21105,#21106,#21107,#21108,#21109,#21110,#21111,#21112,#21113,#21114,
#21115,#21116,#21117,#21118,#21119,#21120,#21121,#21122,#21123,#21124,#21125,
#21126,#21127,#21128,#21129,#21130,#21131),.UNSPECIFIED.,.F.,.F.,(4,2,2,
2,2,2,2,2,2,2,2,2,2,2,2,2,2,2,2,2,2,2,2,2,2,2,2,2,2,2,2,2,2,2,2,2,2,2,2,
2,2,2,2,2,2,2,2,2,2,2,2,2,2,2,4),(-4.05879903554358,-3.99554088987618,-3.98621912338381,
-3.98503812881777,-3.98429819559836,-3.98360668770163,-3.98304637835795,
-3.98239618382111,-3.98128120791761,-3.97712723929307,-3.90870012322013,
-3.89521413325899,-3.88194115673587,-3.84409423659441,-3.82737011219942,
-3.8252062298073,-3.82385799780418,-3.82259940454519,-3.82168779637406,
-3.82071676951049,-3.81906151916928,-3.81457777495714,-3.7416071005807,
-3.71739937374859,-3.6918251124252,-3.67155298878052,-3.66582267743168,
-3.66233178819508,-3.66158159881658,-3.66088271451388,-3.6603218979078,
-3.65967722540041,-3.65858593458801,-3.65466124682145,-3.58976116230847,
-3.5406275262575,-3.50903661801502,-3.50249712733391,-3.50113652069968,
-3.49986898133139,-3.49895612217392,-3.4979886247264,-3.49662632269505,
-3.49380572196624,-3.48622776825605,-3.48441706283362,-3.4823554363696,
-3.48188080183464,-3.48103750001944,-3.47700410389334,-3.47580949027072,
-3.4743142426484,-3.46972980628327,-3.42460957868219,-3.39850283521087),
 .UNSPECIFIED.);
#126=B_SPLINE_CURVE_WITH_KNOTS('',3,(#21132,#21133,#21134,#21135,#21136,
#21137,#21138,#21139,#21140,#21141,#21142,#21143,#21144,#21145,#21146,#21147,
#21148,#21149,#21150,#21151,#21152,#21153,#21154,#21155,#21156,#21157,#21158,
#21159,#21160,#21161,#21162,#21163,#21164,#21165,#21166,#21167,#21168,#21169,
#21170,#21171,#21172,#21173,#21174,#21175,#21176,#21177,#21178,#21179,#21180,
#21181,#21182,#21183,#21184,#21185,#21186,#21187,#21188,#21189,#21190,#21191,
#21192,#21193,#21194,#21195,#21196,#21197,#21198,#21199,#21200,#21201,#21202,
#21203,#21204,#21205,#21206,#21207,#21208,#21209,#21210,#21211,#21212,#21213,
#21214,#21215,#21216,#21217,#21218,#21219,#21220,#21221,#21222,#21223,#21224,
#21225,#21226,#21227,#21228,#21229,#21230,#21231,#21232,#21233,#21234,#21235,
#21236,#21237,#21238,#21239,#21240,#21241,#21242,#21243,#21244,#21245,#21246,
#21247,#21248,#21249,#21250,#21251,#21252,#21253,#21254,#21255,#21256,#21257,
#21258,#21259,#21260,#21261,#21262,#21263,#21264,#21265,#21266,#21267,#21268,
#21269,#21270,#21271,#21272,#21273,#21274,#21275,#21276,#21277,#21278,#21279,
#21280,#21281,#21282,#21283,#21284,#21285,#21286,#21287,#21288,#21289,#21290,
#21291,#21292,#21293,#21294,#21295,#21296,#21297,#21298,#21299,#21300,#21301,
#21302,#21303,#21304,#21305,#21306,#21307,#21308,#21309,#21310,#21311,#21312,
#21313,#21314,#21315,#21316,#21317,#21318,#21319,#21320,#21321,#21322,#21323,
#21324,#21325,#21326,#21327,#21328,#21329,#21330,#21331,#21332,#21333,#21334,
#21335,#21336,#21337,#21338,#21339,#21340,#21341,#21342,#21343,#21344,#21345,
#21346,#21347,#21348,#21349,#21350,#21351,#21352,#21353,#21354,#21355,#21356,
#21357,#21358,#21359,#21360,#21361,#21362,#21363,#21364,#21365,#21366,#21367,
#21368,#21369,#21370,#21371,#21372,#21373,#21374,#21375,#21376,#21377,#21378,
#21379,#21380,#21381,#21382,#21383,#21384,#21385,#21386,#21387,#21388,#21389,
#21390,#21391,#21392,#21393,#21394,#21395,#21396,#21397,#21398,#21399,#21400,
#21401,#21402,#21403,#21404,#21405,#21406,#21407,#21408,#21409,#21410,#21411,
#21412,#21413,#21414,#21415,#21416,#21417,#21418,#21419),.UNSPECIFIED.,
 .F.,.F.,(4,2,2,2,2,2,2,2,2,2,2,2,2,2,2,2,2,2,2,2,2,2,2,2,2,2,2,2,2,2,2,
2,2,2,2,2,2,2,2,2,2,2,2,2,2,2,2,2,2,2,2,2,2,2,2,2,2,2,2,2,2,2,2,2,2,2,2,
2,2,2,2,2,2,2,2,2,2,2,2,2,2,2,2,2,2,2,2,2,2,2,2,2,2,2,2,2,2,2,2,2,2,2,2,
2,2,2,2,2,2,2,2,2,2,2,2,2,2,2,2,2,2,2,2,2,2,2,2,2,2,2,2,2,2,2,2,2,2,2,2,
2,2,2,2,4),(-2.69197257292336,-2.68558870129701,-2.66197432596306,-2.65732281965966,
-2.65620475698648,-2.65556017445217,-2.65499888971945,-2.65429871859818,
-2.65321677820789,-2.6482947366379,-2.55263675802256,-2.49984122693837,
-2.49739779419988,-2.49593251052439,-2.49460753532955,-2.4936063254273,
-2.49265165286103,-2.49133892620616,-2.48801813592373,-2.44567859191875,
-2.39872534191373,-2.37499323447793,-2.3362198199124,-2.33381717772997,
-2.33293929681208,-2.33234804835674,-2.33177462881831,-2.33108347569428,
-2.32935883503651,-2.31358264844087,-2.31036822500928,-2.25628471440178,
-2.21082490355755,-2.18700079132994,-2.17492369987761,-2.1726764694906,
-2.1714661553163,-2.17047126273508,-2.16945255230329,-2.16756151098957,
-2.16133698384822,-2.05444444382153,-2.03064192808659,-2.02911065115783,
-2.02652218651379,-2.02593947813371,-2.01212372440356,-2.01062498993237,
-2.00988425790518,-2.0093502659947,-2.00877969844171,-2.00800814222508,
-2.00626328234132,-1.96524687361196,-1.85708769983655,-1.85095311777042,
-1.84907282605336,-1.84805628217632,-1.84705163282641,-1.8458337094549,
-1.84355097253,-1.83077785636157,-1.80597512459368,-1.71619481115066,-1.6893468850248,
-1.68742236962878,-1.68667810568068,-1.68614319260008,-1.68557322423781,
-1.6848051389134,-1.68312046652754,-1.68085309042961,-1.6590548811644,-1.63514327775534,
-1.55139690222005,-1.52956577859469,-1.52672439216678,-1.52538691167949,
-1.52436610645546,-1.52327862093308,-1.52158671018237,-1.51652232160609,
-1.45628053824052,-1.38467312540276,-1.38300216294716,-1.38212046344854,
-1.38100624156066,-1.38011864633581,-1.37977223855767,-1.37884347203643,
-1.37839978712563,-1.37762182981665,-1.36577082316945,-1.36433508942931,
-1.36361024735128,-1.36308043411033,-1.3625070581423,-1.36171919124365,
-1.35992603610337,-1.35747595786608,-1.26852972763752,-1.20788237429976,
-1.20409557524715,-1.20270717231946,-1.20173215053389,-1.20082098680541,
-1.19956953811251,-1.19718005917181,-1.18175771447576,-1.14627263588776,
-1.08547717658398,-1.04406229685018,-1.04155987831136,-1.04063639832981,
-1.04009526286447,-1.03958522583693,-1.03886899605185,-1.03753216136736,
-1.02793239847405,-1.00368360305475,-0.948181389592564,-0.885069889383899,
-0.881191899349148,-0.879789513393375,-0.87881063862359,-0.877900579757035,
-0.87665789336991,-0.874321858833368,-0.860604748253787,-0.83329142814411,
-0.775457946310528,-0.730581824977383,-0.719733106799663,-0.718333429689929,
-0.717617822010414,-0.717090399030972,-0.716515165503138,-0.715716956764076,
-0.713867675680136,-0.711320399142619,-0.70481222419764,-0.696070547323417,
-0.684622170995794,-0.66165633052871),.UNSPECIFIED.);
#127=B_SPLINE_CURVE_WITH_KNOTS('',3,(#21424,#21425,#21426,#21427,#21428,
#21429,#21430,#21431,#21432,#21433,#21434,#21435,#21436,#21437,#21438,#21439,
#21440,#21441,#21442,#21443,#21444,#21445,#21446,#21447,#21448,#21449,#21450,
#21451,#21452,#21453,#21454,#21455,#21456,#21457,#21458,#21459,#21460,#21461,
#21462,#21463,#21464,#21465,#21466,#21467,#21468,#21469,#21470,#21471,#21472,
#21473,#21474,#21475,#21476,#21477,#21478,#21479,#21480,#21481,#21482,#21483,
#21484,#21485,#21486,#21487,#21488,#21489,#21490,#21491,#21492,#21493,#21494,
#21495,#21496,#21497,#21498,#21499,#21500,#21501,#21502,#21503,#21504,#21505,
#21506,#21507,#21508,#21509,#21510,#21511,#21512,#21513,#21514,#21515,#21516,
#21517,#21518,#21519,#21520,#21521,#21522,#21523,#21524,#21525,#21526,#21527,
#21528,#21529,#21530,#21531,#21532,#21533,#21534,#21535,#21536,#21537,#21538,
#21539,#21540,#21541,#21542,#21543,#21544,#21545,#21546,#21547,#21548,#21549,
#21550,#21551,#21552,#21553,#21554,#21555,#21556,#21557,#21558,#21559,#21560,
#21561,#21562,#21563,#21564,#21565,#21566,#21567,#21568,#21569,#21570,#21571,
#21572,#21573,#21574,#21575,#21576,#21577,#21578,#21579,#21580,#21581,#21582,
#21583,#21584,#21585,#21586,#21587,#21588,#21589,#21590,#21591,#21592,#21593,
#21594,#21595,#21596,#21597,#21598,#21599,#21600,#21601,#21602,#21603,#21604,
#21605,#21606,#21607,#21608,#21609,#21610,#21611,#21612,#21613,#21614,#21615,
#21616,#21617,#21618,#21619,#21620,#21621,#21622,#21623,#21624,#21625,#21626,
#21627,#21628,#21629,#21630,#21631,#21632,#21633,#21634,#21635,#21636,#21637,
#21638,#21639,#21640,#21641,#21642,#21643,#21644,#21645,#21646,#21647,#21648,
#21649,#21650,#21651,#21652,#21653,#21654,#21655,#21656,#21657,#21658,#21659,
#21660,#21661,#21662,#21663,#21664,#21665,#21666,#21667,#21668,#21669,#21670,
#21671,#21672,#21673,#21674,#21675,#21676,#21677,#21678,#21679,#21680,#21681,
#21682,#21683,#21684,#21685,#21686,#21687,#21688,#21689,#21690,#21691,#21692,
#21693,#21694,#21695,#21696,#21697,#21698,#21699,#21700,#21701,#21702,#21703,
#21704,#21705,#21706,#21707,#21708,#21709,#21710,#21711,#21712,#21713,#21714,
#21715,#21716,#21717,#21718,#21719,#21720,#21721,#21722,#21723,#21724,#21725,
#21726,#21727,#21728,#21729,#21730,#21731,#21732,#21733,#21734,#21735),
 .UNSPECIFIED.,.F.,.F.,(4,2,2,2,2,2,2,2,2,2,2,2,2,2,2,2,2,2,2,2,2,2,2,2,
2,2,2,2,2,2,2,2,2,2,2,2,2,2,2,2,2,2,2,2,2,2,2,2,2,2,2,2,2,2,2,2,2,2,2,2,
2,2,2,2,2,2,2,2,2,2,2,2,2,2,2,2,2,2,2,2,2,2,2,2,2,2,2,2,2,2,2,2,2,2,2,2,
2,2,2,2,2,2,2,2,2,2,2,2,2,2,2,2,2,2,2,2,2,2,2,2,2,2,2,2,2,2,2,2,2,2,2,2,
2,2,2,2,2,2,2,2,2,2,2,2,2,2,2,2,2,2,2,2,2,2,2,4),(-3.39994190379461,-3.36686671547447,
-3.3353143830966,-3.32088860049697,-3.31851875602958,-3.31728242357063,
-3.31637324834893,-3.31539169536757,-3.31368516309039,-3.30886169714366,
-3.23465097473941,-3.18488367286284,-3.16591242973773,-3.16034992324727,
-3.15693752967021,-3.15593522920706,-3.1553119929754,-3.15474703411569,
-3.15402406301256,-3.15249496903317,-3.14223517336176,-3.11168002817093,
-3.04859834456225,-3.01783989468509,-2.99824871151382,-2.99570139463886,
-2.99442829638924,-2.99351421204596,-2.99254798202207,-2.99119165018948,
-2.98839694551298,-2.95932544966547,-2.94092748259092,-2.88926552585634,
-2.83712026523338,-2.83399167194498,-2.83301979899301,-2.83240351614683,
-2.8318365067624,-2.83109951512332,-2.8295545202872,-2.81845345414458,-2.81706355541898,
-2.81543496704861,-2.8123635238008,-2.80950952767162,-2.79962581751556,
-2.7208056509041,-2.68047808446914,-2.67625076409714,-2.6730904645732,-2.67169993695668,
-2.67067429421303,-2.66972579526836,-2.66843675721008,-2.6652535811524,
-2.63029675143227,-2.62598101683703,-2.55653590222699,-2.53454206936298,
-2.51432613623547,-2.51106838865576,-2.51008401004515,-2.50946487433436,
-2.50889877342128,-2.50816776951067,-2.50659679170939,-2.49534468176697,
-2.39767689545897,-2.35743677085424,-2.35105242774565,-2.34920988297564,
-2.34808896687107,-2.34707865085006,-2.34579079668514,-2.34317002487223,
-2.32732565526589,-2.32605362037779,-2.32484356954319,-2.32335734684001,
-2.31793892446429,-2.31107748677495,-2.2201415332063,-2.19777364778313,
-2.18862767193993,-2.187268558565,-2.1865720666893,-2.18601112699911,-2.18536402764059,
-2.18426332121985,-2.18025267640077,-2.17978475919677,-2.07644517793773,
-2.03106152580403,-2.027288211116,-2.02590209091859,-2.02492783924187,-2.02401673205298,
-2.02276433029175,-2.02031723875477,-2.00358819772434,-1.96317906022367,
-1.86996907063978,-1.86539299402114,-1.86421448054179,-1.86349249576684,
-1.86292765753868,-1.86230386418786,-1.86127861082753,-1.85765838314073,
-1.776143950284,-1.73096656151708,-1.72666906629073,-1.72462057014749,-1.72341556570895,
-1.72191617834342,-1.7198341138536,-1.71922605406235,-1.71777617153632,
-1.71717606508104,-1.71543648900971,-1.71155567855791,-1.70503258657368,
-1.70310681812096,-1.70196719615696,-1.7010606744472,-1.69984978381114,
-1.69764462865564,-1.68622134319837,-1.66388713706814,-1.6197904993009,
-1.56402705404717,-1.5613312353022,-1.55976279743349,-1.55900937887274,
-1.54310235539281,-1.54137404069008,-1.54068229855055,-1.54010873964246,
-1.5395177235168,-1.53864086524163,-1.53630061824498,-1.47992250780356,
-1.40229277090721,-1.39874793901543,-1.39668724913639,-1.3928877448191,
-1.38932053123187,-1.38787135919095,-1.38195088094742,-1.38009682707836,
-1.37908563541282,-1.37808067429462,-1.37685425645365,-1.37457771026683,
-1.3699358201607),.UNSPECIFIED.);
#128=B_SPLINE_CURVE_WITH_KNOTS('',3,(#21737,#21738,#21739,#21740,#21741,
#21742,#21743,#21744,#21745,#21746,#21747,#21748,#21749,#21750,#21751,#21752,
#21753,#21754,#21755,#21756,#21757,#21758,#21759,#21760,#21761,#21762,#21763,
#21764,#21765,#21766,#21767,#21768,#21769,#21770,#21771,#21772,#21773,#21774,
#21775,#21776,#21777,#21778,#21779,#21780,#21781,#21782,#21783,#21784,#21785,
#21786,#21787,#21788,#21789,#21790,#21791,#21792,#21793,#21794,#21795,#21796,
#21797,#21798,#21799,#21800,#21801,#21802,#21803,#21804,#21805,#21806,#21807,
#21808,#21809,#21810,#21811,#21812,#21813,#21814,#21815,#21816,#21817,#21818,
#21819,#21820,#21821,#21822,#21823,#21824,#21825,#21826,#21827,#21828,#21829,
#21830,#21831,#21832,#21833,#21834,#21835,#21836),.UNSPECIFIED.,.F.,.F.,
(4,2,2,2,2,2,2,2,2,2,2,2,2,2,2,2,2,2,2,2,2,2,2,2,2,2,2,2,2,2,2,2,2,2,2,
2,2,2,2,2,2,2,2,2,2,2,2,2,2,4),(-0.66165633052871,-0.635984384500012,-0.562974439167031,
-0.55846545761205,-0.556805679247827,-0.555833318267037,-0.554921310569708,
-0.553663501486698,-0.552316608348213,-0.54600727273951,-0.512179291842036,
-0.460240222757477,-0.399721702144545,-0.395981677764637,-0.394897181874368,
-0.394323694392617,-0.393819559522827,-0.393163399143196,-0.392472969700445,
-0.389819399905494,-0.385801683552211,-0.373690020797935,-0.343571448335568,
-0.31846175840726,-0.283613520019905,-0.267874805845795,-0.238065132715674,
-0.235252396569741,-0.233891513264224,-0.232923946812276,-0.232010148828416,
-0.230739917280611,-0.229375868741327,-0.227175090855721,-0.210421535739774,
-0.169549262745376,-0.155229153504232,-0.140886456995155,-0.0865925462122985,
-0.085810963723819,-0.0739648514776291,-0.0725293002386787,-0.0718045093759444,
-0.0712747139713807,-0.070701337578965,-0.0699134359344539,-0.0690395041762753,
-0.0675348758374232,-0.0643468711601317,-0.00096143554933532),
 .UNSPECIFIED.);
#129=B_SPLINE_CURVE_WITH_KNOTS('',3,(#21837,#21838,#21839,#21840,#21841,
#21842,#21843,#21844,#21845,#21846,#21847,#21848,#21849,#21850,#21851,#21852,
#21853,#21854,#21855,#21856,#21857,#21858,#21859,#21860,#21861,#21862,#21863,
#21864,#21865,#21866,#21867,#21868,#21869,#21870,#21871,#21872,#21873,#21874,
#21875,#21876,#21877,#21878,#21879,#21880,#21881,#21882,#21883,#21884,#21885,
#21886,#21887,#21888,#21889,#21890,#21891,#21892,#21893,#21894,#21895,#21896,
#21897,#21898,#21899,#21900,#21901,#21902,#21903,#21904,#21905,#21906,#21907,
#21908,#21909,#21910,#21911,#21912,#21913,#21914,#21915,#21916,#21917,#21918,
#21919,#21920,#21921,#21922,#21923,#21924,#21925,#21926,#21927,#21928,#21929,
#21930,#21931,#21932,#21933,#21934,#21935,#21936,#21937,#21938,#21939,#21940,
#21941,#21942,#21943,#21944,#21945,#21946,#21947,#21948,#21949,#21950,#21951,
#21952,#21953,#21954,#21955,#21956,#21957,#21958,#21959,#21960,#21961,#21962,
#21963,#21964,#21965,#21966,#21967,#21968,#21969,#21970,#21971,#21972,#21973,
#21974,#21975,#21976,#21977,#21978,#21979,#21980,#21981,#21982,#21983,#21984,
#21985,#21986,#21987,#21988,#21989,#21990,#21991,#21992,#21993,#21994,#21995,
#21996,#21997,#21998,#21999,#22000,#22001,#22002,#22003,#22004,#22005,#22006,
#22007,#22008,#22009,#22010,#22011,#22012,#22013,#22014,#22015,#22016,#22017,
#22018,#22019,#22020,#22021,#22022),.UNSPECIFIED.,.F.,.F.,(4,2,2,2,2,2,
2,2,2,2,2,2,2,2,2,2,2,2,2,2,2,2,2,2,2,2,2,2,2,2,2,2,2,2,2,2,2,2,2,2,2,2,
2,2,2,2,2,2,2,2,2,2,2,2,2,2,2,2,2,2,2,2,2,2,2,2,2,2,2,2,2,2,2,2,2,2,2,2,
2,2,2,2,2,2,2,2,2,2,2,2,2,2,4),(-4.06047580903049,-3.98883313326063,-3.97433174222971,
-3.97231615819279,-3.97103026322687,-3.96981660773599,-3.9689101138855,
-3.96791765123857,-3.96615558855538,-3.96093779637892,-3.87982606029779,
-3.86711580617506,-3.85513990465006,-3.82410279092963,-3.81045430326376,
-3.80939165982954,-3.80870133594423,-3.80804533399209,-3.80754143495988,
-3.80696833782391,-3.80588493988309,-3.80215190100195,-3.74191149701363,
-3.70677328960837,-3.66727014731604,-3.65078911791453,-3.64906328254663,
-3.64753294432398,-3.64648057880591,-3.64545111107353,-3.64421233997431,
-3.64112862306226,-3.61281424433995,-3.5955781109469,-3.56064874121213,
-3.5133444215052,-3.4879053506647,-3.48626766082138,-3.48567275931329,-3.48508275686296,
-3.48450875733961,-3.48381483723945,-3.48214040520487,-3.46729561720466,
-3.46590327425025,-3.46492562397453,-3.46331580987113,-3.425703124508,-3.37740946237235,
-3.34309732977652,-3.3331423515119,-3.32695868926105,-3.32562004072067,
-3.32436829888795,-3.32345741237483,-3.32248315168608,-3.32081240291859,
-3.31622857999019,-3.24619217601516,-3.19027105678354,-3.1728249390854,
-3.16461403063333,-3.16329556551346,-3.16260203825595,-3.16209519610309,
-3.16154471064184,-3.16057361738588,-3.15774124008521,-3.11245370346695,
-3.05411473487646,-3.03178403192391,-3.00612640876865,-3.00314283346351,
-3.00176982781755,-3.00074735164778,-2.99979478305143,-2.99848937510751,
-2.99521015756728,-2.95532292213387,-2.90218565081376,-2.86662338193906,
-2.84999521019353,-2.8418396676274,-2.84052324068034,-2.83996270506864,
-2.83939335217304,-2.83885807977053,-2.83811188456463,-2.83617445442692,
-2.80846934513124,-2.74391432612601,-2.69999660334342,-2.69216032599444),
 .UNSPECIFIED.);
#130=B_SPLINE_CURVE_WITH_KNOTS('',3,(#22028,#22029,#22030,#22031,#22032,
#22033,#22034,#22035,#22036,#22037,#22038,#22039,#22040,#22041,#22042,#22043,
#22044,#22045,#22046,#22047,#22048,#22049,#22050,#22051,#22052,#22053,#22054,
#22055,#22056,#22057,#22058,#22059,#22060,#22061,#22062,#22063,#22064,#22065,
#22066,#22067,#22068,#22069,#22070,#22071,#22072,#22073,#22074,#22075,#22076,
#22077,#22078,#22079,#22080,#22081,#22082,#22083,#22084,#22085,#22086,#22087,
#22088,#22089,#22090,#22091,#22092,#22093,#22094,#22095,#22096,#22097,#22098,
#22099,#22100,#22101,#22102,#22103,#22104,#22105,#22106,#22107,#22108,#22109,
#22110,#22111,#22112,#22113,#22114,#22115,#22116,#22117,#22118,#22119,#22120,
#22121,#22122,#22123,#22124,#22125,#22126,#22127,#22128,#22129,#22130,#22131,
#22132,#22133,#22134,#22135,#22136,#22137,#22138,#22139,#22140,#22141,#22142,
#22143,#22144,#22145,#22146,#22147,#22148,#22149,#22150,#22151,#22152,#22153,
#22154,#22155,#22156,#22157,#22158,#22159,#22160,#22161,#22162,#22163,#22164,
#22165,#22166,#22167,#22168,#22169,#22170,#22171,#22172,#22173,#22174,#22175,
#22176,#22177,#22178,#22179,#22180,#22181,#22182,#22183,#22184,#22185,#22186,
#22187,#22188,#22189,#22190,#22191,#22192,#22193,#22194,#22195,#22196,#22197,
#22198,#22199,#22200,#22201,#22202,#22203,#22204,#22205,#22206,#22207,#22208,
#22209,#22210,#22211,#22212,#22213,#22214,#22215,#22216,#22217,#22218,#22219,
#22220,#22221,#22222,#22223,#22224,#22225,#22226,#22227,#22228,#22229,#22230,
#22231,#22232,#22233,#22234,#22235,#22236,#22237,#22238,#22239,#22240,#22241,
#22242,#22243,#22244,#22245,#22246,#22247),.UNSPECIFIED.,.F.,.F.,(4,2,2,
2,2,2,2,2,2,2,2,2,2,2,2,2,2,2,2,2,2,2,2,2,2,2,2,2,2,2,2,2,2,2,2,2,2,2,2,
2,2,2,2,2,2,2,2,2,2,2,2,2,2,2,2,2,2,2,2,2,2,2,2,2,2,2,2,2,2,2,2,2,2,2,2,
2,2,2,2,2,2,2,2,2,2,2,2,2,2,2,2,2,2,2,2,2,2,2,2,2,2,2,2,2,2,2,2,2,2,4),
(-1.36933136652665,-1.35859732837197,-1.35679844377335,-1.3560756299863,
-1.35554637601637,-1.35497267364315,-1.35419864345503,-1.35242748297969,
-1.35001542973958,-1.29723606513501,-1.23799221414758,-1.2202622694919,
-1.19902079686839,-1.1961645522769,-1.19484476680884,-1.19382686061541,
-1.19273205156696,-1.19100700614308,-1.18567401504065,-1.15554947806589,
-1.08392996334039,-1.03702220569548,-1.03420218753497,-1.0332327701601,
-1.03268247099359,-1.0321753118985,-1.03163529287504,-1.03052243514212,
-1.02591438107519,-0.986920138840623,-0.941386962772281,-0.877672530167167,
-0.873749491490016,-0.872340260322915,-0.871359481999703,-0.870449906166499,
-0.869211323069769,-0.86683139099472,-0.852481402160477,-0.834722860015409,
-0.79528494363612,-0.754802711299645,-0.713568240721987,-0.711147339135666,
-0.710328017645314,-0.709772443060438,-0.709266430859045,-0.708729123885893,
-0.708058962826953,-0.705648388506033,-0.702093570402397,-0.691843265438953,
-0.651595348269289,-0.623878390672399,-0.59084091278337,-0.578798136419498,
-0.572594587476458,-0.571198852570911,-0.569993318363737,-0.568512451345134,
-0.566427324196033,-0.565844930417326,-0.5641022026392,-0.563076093071555,
-0.561496730412553,-0.556726341606073,-0.551340673535203,-0.54955529351537,
-0.548557801069253,-0.547560445768462,-0.546312955568382,-0.543890556503511,
-0.528720613115969,-0.49936180784944,-0.491941695176374,-0.445450396081606,
-0.401591305535271,-0.389481453388935,-0.387877094519413,-0.387139706156022,
-0.386572570986094,-0.385956335709198,-0.385322617974015,-0.384395670430321,
-0.376732035161832,-0.360961361345349,-0.338245353325395,-0.317451678039698,
-0.233796636418477,-0.228371867418463,-0.22658133227778,-0.22558284130101,
-0.224585720923131,-0.22334036572751,-0.220927982166584,-0.205857449705273,
-0.158454538121891,-0.142348808427161,-0.134443639150519,-0.125493795394888,
-0.0690603051038075,-0.0655771059460002,-0.0645222179554844,-0.0639547035293388,
-0.0633941699555315,-0.0628556305844188,-0.0621810628609401,-0.0611562183700187,
-0.0592733000428786,-0.000961179395231121),.UNSPECIFIED.);
#131=B_SPLINE_CURVE_WITH_KNOTS('',3,(#22248,#22249,#22250,#22251,#22252,
#22253,#22254,#22255,#22256,#22257,#22258,#22259,#22260,#22261,#22262,#22263,
#22264,#22265,#22266,#22267,#22268,#22269,#22270,#22271,#22272,#22273,#22274,
#22275,#22276,#22277,#22278,#22279,#22280,#22281,#22282,#22283,#22284,#22285,
#22286,#22287,#22288,#22289,#22290,#22291,#22292,#22293,#22294,#22295,#22296,
#22297,#22298,#22299,#22300,#22301,#22302,#22303,#22304,#22305,#22306,#22307,
#22308,#22309,#22310,#22311,#22312,#22313,#22314,#22315,#22316,#22317,#22318,
#22319,#22320,#22321,#22322,#22323,#22324,#22325,#22326,#22327,#22328,#22329,
#22330,#22331,#22332,#22333,#22334,#22335,#22336,#22337,#22338,#22339),
 .UNSPECIFIED.,.F.,.F.,(4,2,2,2,2,2,2,2,2,2,2,2,2,2,2,2,2,2,2,2,2,2,2,2,
2,2,2,2,2,2,2,2,2,2,2,2,2,2,2,2,2,2,2,2,2,4),(-4.06120382105492,-3.97640958314511,
-3.96975879707925,-3.96672639584915,-3.96430994746887,-3.96306390334572,
-3.9621535973804,-3.96117656644359,-3.9597803792858,-3.95594182519937,-3.89726557700427,
-3.86480146420021,-3.84329555144617,-3.81339687041797,-3.80343721157549,
-3.80245568316642,-3.80179931577592,-3.80116733848241,-3.80060440339047,
-3.79988535767731,-3.79846392784794,-3.79005022970795,-3.78938383091348,
-3.74400169621109,-3.72002255434853,-3.69601452988427,-3.65958898768583,
-3.64391669635236,-3.64149710214395,-3.64025038758376,-3.63925332739859,
-3.63825585745862,-3.63646977753036,-3.63107681825785,-3.54785806701969,
-3.5071706777738,-3.48213777894182,-3.47963593964031,-3.47895828503783,
-3.47841890659564,-3.4779120817863,-3.47736088245231,-3.47638665970961,
-3.47353389442328,-3.42479367187728,-3.39994190379461),.UNSPECIFIED.);
#132=B_SPLINE_CURVE_WITH_KNOTS('',3,(#22340,#22341,#22342,#22343,#22344,
#22345,#22346,#22347,#22348,#22349,#22350,#22351,#22352,#22353,#22354,#22355,
#22356,#22357,#22358,#22359,#22360,#22361,#22362,#22363,#22364,#22365,#22366,
#22367,#22368,#22369,#22370,#22371,#22372,#22373,#22374,#22375,#22376,#22377,
#22378,#22379,#22380,#22381,#22382,#22383,#22384,#22385,#22386,#22387,#22388,
#22389,#22390,#22391,#22392,#22393,#22394,#22395,#22396,#22397,#22398,#22399,
#22400,#22401,#22402,#22403,#22404,#22405,#22406,#22407,#22408,#22409,#22410,
#22411,#22412,#22413,#22414,#22415,#22416,#22417,#22418,#22419,#22420,#22421,
#22422,#22423,#22424,#22425,#22426,#22427,#22428,#22429,#22430,#22431,#22432,
#22433,#22434,#22435,#22436,#22437,#22438,#22439,#22440,#22441,#22442,#22443,
#22444,#22445,#22446,#22447,#22448,#22449,#22450,#22451,#22452,#22453,#22454,
#22455,#22456,#22457,#22458,#22459,#22460,#22461,#22462,#22463,#22464,#22465,
#22466,#22467,#22468,#22469,#22470,#22471,#22472,#22473,#22474,#22475,#22476,
#22477,#22478,#22479,#22480,#22481,#22482,#22483,#22484,#22485,#22486,#22487,
#22488,#22489,#22490,#22491,#22492,#22493,#22494,#22495,#22496,#22497,#22498,
#22499,#22500,#22501,#22502,#22503,#22504,#22505,#22506,#22507,#22508,#22509,
#22510,#22511,#22512,#22513,#22514,#22515,#22516,#22517,#22518,#22519,#22520,
#22521,#22522,#22523,#22524,#22525,#22526,#22527,#22528,#22529,#22530,#22531,
#22532,#22533,#22534,#22535,#22536,#22537,#22538,#22539,#22540,#22541,#22542,
#22543,#22544,#22545,#22546,#22547,#22548,#22549,#22550,#22551,#22552,#22553,
#22554,#22555,#22556,#22557,#22558,#22559,#22560,#22561,#22562,#22563,#22564,
#22565,#22566,#22567,#22568,#22569,#22570,#22571,#22572,#22573,#22574,#22575,
#22576,#22577,#22578,#22579,#22580,#22581,#22582,#22583,#22584,#22585,#22586,
#22587,#22588,#22589,#22590,#22591,#22592,#22593,#22594,#22595,#22596,#22597,
#22598,#22599,#22600,#22601,#22602,#22603,#22604,#22605,#22606,#22607,#22608,
#22609,#22610,#22611,#22612,#22613,#22614,#22615),.UNSPECIFIED.,.F.,.F.,
(4,2,2,2,2,2,2,2,2,2,2,2,2,2,2,2,2,2,2,2,2,2,2,2,2,2,2,2,2,2,2,2,2,2,2,
2,2,2,2,2,2,2,2,2,2,2,2,2,2,2,2,2,2,2,2,2,2,2,2,2,2,2,2,2,2,2,2,2,2,2,2,
2,2,2,2,2,2,2,2,2,2,2,2,2,2,2,2,2,2,2,2,2,2,2,2,2,2,2,2,2,2,2,2,2,2,2,2,
2,2,2,2,2,2,2,2,2,2,2,2,2,2,2,2,2,2,2,2,2,2,2,2,2,2,2,2,2,2,4),(-2.69216032599444,
-2.68256417590344,-2.68007713642079,-2.6788062022544,-2.67789264630646,
-2.67692602743868,-2.67556760439536,-2.67276359534767,-2.64327892100576,
-2.57086876165611,-2.52042625896441,-2.5181422908361,-2.51728383272484,
-2.51669308696804,-2.51611956159346,-2.51542759662574,-2.51369733528641,
-2.49771168508564,-2.41046215113946,-2.37493365698338,-2.35950229976759,
-2.35711082110835,-2.35585997463697,-2.35494919890404,-2.35397454470261,
-2.35258658412885,-2.34880049841245,-2.2880662356285,-2.19930509586882,
-2.19680480713766,-2.19496902789737,-2.19418144646227,-2.19360827039963,
-2.19307863629407,-2.1923540315637,-2.1909187478434,-2.17907073651276,-2.12977394733911,
-2.08031455149015,-2.04176552373685,-2.03764833910232,-2.03455448358542,
-2.03317608994889,-2.03215261015968,-2.03120126284038,-2.02964907861517,
-2.02550019593995,-1.97134839628577,-1.87763228495316,-1.87283790101063,
-1.87176629945954,-1.87106939154301,-1.87050841205929,-1.86986159689154,
-1.86873325614486,-1.86394951813639,-1.80911394186765,-1.74311979734322,
-1.71462403543459,-1.71153454203009,-1.71029458016937,-1.70926456707442,
-1.70821209800044,-1.70668243512435,-1.70277420196482,-1.65350355853836,
-1.56391901330394,-1.56218150430741,-1.55047099935864,-1.54904016339376,
-1.54831657964489,-1.54778710342285,-1.547213504572,-1.5464402249623,-1.54467402977646,
-1.5422700451172,-1.46078336800303,-1.41563364008452,-1.41121782448186,
-1.4096041767702,-1.40840915117971,-1.4045518372305,-1.40409700130604,-1.39063331823151,
-1.38839187943923,-1.38705736102138,-1.38603704690316,-1.38494836940782,
-1.38325107425292,-1.37814516105983,-1.31782573627011,-1.2524940840427,
-1.24879604868922,-1.24368515122984,-1.22766826844726,-1.22593662829394,
-1.22524427368686,-1.22467048991183,-1.22407954653552,-1.22322096294083,
-1.22095467146577,-1.17183282655734,-1.11892842194507,-1.09893475995475,
-1.06867398955178,-1.06585070310348,-1.06448723373829,-1.06351896770124,
-1.06260543310214,-1.06133703451081,-1.05888273429333,-1.04148420725421,
-0.998092735258393,-0.9462339516449,-0.922939634532858,-0.92100927969179,
-0.904769821228077,-0.903204833015748,-0.902447730867808,-0.901909374934994,
-0.901398145291054,-0.900674195685458,-0.899210215999472,-0.886232376356095,
-0.861009631202176,-0.816054798288133,-0.781907803041267,-0.745979175078631,
-0.742774989588326,-0.741482132788039,-0.740532510972375,-0.739507269624768,
-0.738120140040361,-0.735078190385059,-0.730994764849574,-0.721074799918885,
-0.68696880144044,-0.662395452864075),.UNSPECIFIED.);
#133=B_SPLINE_CURVE_WITH_KNOTS('',3,(#22620,#22621,#22622,#22623,#22624,
#22625,#22626,#22627,#22628,#22629,#22630,#22631,#22632,#22633,#22634,#22635,
#22636,#22637,#22638,#22639,#22640,#22641,#22642,#22643,#22644,#22645,#22646,
#22647,#22648,#22649,#22650,#22651,#22652,#22653,#22654,#22655,#22656,#22657,
#22658,#22659,#22660,#22661,#22662,#22663,#22664,#22665,#22666,#22667,#22668,
#22669,#22670,#22671,#22672,#22673,#22674,#22675,#22676,#22677,#22678,#22679,
#22680,#22681,#22682,#22683,#22684,#22685,#22686,#22687,#22688,#22689,#22690,
#22691,#22692,#22693,#22694,#22695,#22696,#22697,#22698,#22699,#22700,#22701,
#22702,#22703,#22704,#22705,#22706,#22707,#22708,#22709,#22710,#22711,#22712,
#22713,#22714,#22715,#22716,#22717,#22718,#22719,#22720,#22721,#22722,#22723,
#22724,#22725,#22726,#22727,#22728,#22729,#22730,#22731,#22732,#22733,#22734,
#22735,#22736,#22737,#22738,#22739,#22740,#22741,#22742,#22743,#22744,#22745,
#22746,#22747,#22748,#22749,#22750,#22751,#22752,#22753,#22754,#22755,#22756,
#22757,#22758,#22759,#22760,#22761,#22762,#22763,#22764,#22765,#22766,#22767,
#22768,#22769,#22770,#22771,#22772,#22773,#22774,#22775,#22776,#22777,#22778,
#22779,#22780,#22781,#22782,#22783,#22784,#22785,#22786,#22787,#22788,#22789,
#22790,#22791,#22792,#22793,#22794,#22795,#22796,#22797,#22798,#22799,#22800,
#22801,#22802,#22803,#22804,#22805,#22806,#22807,#22808,#22809,#22810,#22811,
#22812,#22813,#22814,#22815,#22816,#22817,#22818,#22819,#22820,#22821,#22822,
#22823,#22824,#22825,#22826,#22827,#22828,#22829,#22830,#22831,#22832,#22833,
#22834,#22835,#22836,#22837,#22838,#22839,#22840,#22841,#22842,#22843,#22844,
#22845,#22846,#22847,#22848,#22849,#22850,#22851,#22852,#22853,#22854,#22855,
#22856,#22857,#22858,#22859,#22860,#22861,#22862,#22863,#22864,#22865,#22866,
#22867,#22868,#22869,#22870,#22871,#22872,#22873,#22874,#22875,#22876,#22877,
#22878,#22879,#22880,#22881,#22882,#22883,#22884,#22885,#22886,#22887,#22888,
#22889,#22890,#22891,#22892,#22893,#22894,#22895,#22896,#22897,#22898,#22899,
#22900,#22901,#22902,#22903,#22904,#22905,#22906,#22907,#22908,#22909),
 .UNSPECIFIED.,.F.,.F.,(4,2,2,2,2,2,2,2,2,2,2,2,2,2,2,2,2,2,2,2,2,2,2,2,
2,2,2,2,2,2,2,2,2,2,2,2,2,2,2,2,2,2,2,2,2,2,2,2,2,2,2,2,2,2,2,2,2,2,2,2,
2,2,2,2,2,2,2,2,2,2,2,2,2,2,2,2,2,2,2,2,2,2,2,2,2,2,2,2,2,2,2,2,2,2,2,2,
2,2,2,2,2,2,2,2,2,2,2,2,2,2,2,2,2,2,2,2,2,2,2,2,2,2,2,2,2,2,2,2,2,2,2,2,
2,2,2,2,2,2,2,2,2,2,2,2,4),(-3.39977149278874,-3.38090444245079,-3.34558587810495,
-3.29698398445742,-3.29513477038172,-3.2943446600453,-3.29377086426373,
-3.29324155046521,-3.29251869404242,-3.29109082141869,-3.27946752807907,
-3.27851113591785,-3.27791993458937,-3.27535674479116,-3.21737635612005,
-3.17205070245837,-3.14839549078539,-3.14053273971339,-3.13709799326763,
-3.13444542537949,-3.13315666524144,-3.13218771724792,-3.1312260803416,
-3.12988740567935,-3.12641208834923,-3.07178887484913,-3.03252891959327,
-2.97764820410214,-2.97286607845193,-2.9717376936666,-2.97109078116529,
-2.97052967304816,-2.96983255046175,-2.96876052033718,-2.96396260594337,
-2.87655431671365,-2.8155400939395,-2.81301730177609,-2.81151909283647,
-2.81016892174822,-2.80916371719404,-2.80821499292269,-2.80692557156988,
-2.80374106149397,-2.76871256812483,-2.6861348869615,-2.67294394698349,
-2.6574246147251,-2.65001321130818,-2.64872593199498,-2.64804444686028,
-2.64748944441994,-2.6469185996763,-2.64584744123566,-2.64222572299929,
-2.64118773642224,-2.64087829827459,-2.54317278266234,-2.49647707131484,
-2.49189195377732,-2.48958879730833,-2.48818188948226,-2.48689864547418,
-2.48590469157775,-2.48493658992919,-2.48357365316847,-2.48075244045645,
-2.4505770359127,-2.43163922203203,-2.36658929029306,-2.32852548778813,
-2.32613335409478,-2.32525692182561,-2.3246659266834,-2.32409217472185,
-2.32339995470954,-2.32166915212564,-2.30568284989736,-2.30441447683426,
-2.30212845782966,-2.2921277586897,-2.24595588792538,-2.20148288131914,
-2.18055017202233,-2.16732336259214,-2.1650184638292,-2.16379570749562,
-2.16288786280276,-2.16189928442285,-2.16015836863715,-2.1550963624773,
-2.14994731037251,-2.14887023577338,-2.14748281520703,-2.14697493512781,
-2.14561049694145,-2.14352001371974,-2.14166729228366,-2.14044159183517,
-2.1386827353804,-2.1310226569701,-2.05564338000376,-2.03051649775536,-2.00495779899638,
-2.00305443343479,-2.00231367367199,-2.00177967169533,-2.0012091033308,
-2.00043756338333,-1.99869281358552,-1.95768226619634,-1.84993839895519,
-1.8434532454316,-1.8415317447069,-1.84039302913161,-1.83948632541065,-1.83827403833674,
-1.83601765734853,-1.82376595128609,-1.79957709990969,-1.75378016684408,
-1.69540852828863,-1.69364875373075,-1.69169087896402,-1.68122655765804,
-1.67984167366494,-1.67912989312402,-1.67860345939771,-1.6780274200856,
-1.67724096301429,-1.67539993296399,-1.67286869204425,-1.58422623865686,
-1.52342992023747,-1.51964633387812,-1.51825851644815,-1.51728372084873,
-1.51637262137671,-1.51512103251473,-1.51267833237566,-1.49731365652859,
-1.46183850426419,-1.38162107220087,-1.37876532622551,-1.36933136652665),
 .UNSPECIFIED.);
#134=B_SPLINE_CURVE_WITH_KNOTS('',3,(#22911,#22912,#22913,#22914,#22915,
#22916,#22917,#22918,#22919,#22920,#22921,#22922,#22923,#22924,#22925,#22926,
#22927,#22928,#22929,#22930,#22931,#22932,#22933,#22934,#22935,#22936,#22937,
#22938,#22939,#22940,#22941,#22942,#22943,#22944,#22945,#22946,#22947,#22948,
#22949,#22950,#22951,#22952,#22953,#22954,#22955,#22956,#22957,#22958,#22959,
#22960,#22961,#22962,#22963,#22964,#22965,#22966,#22967,#22968,#22969,#22970,
#22971,#22972,#22973,#22974,#22975,#22976,#22977,#22978,#22979,#22980,#22981,
#22982,#22983,#22984,#22985,#22986,#22987,#22988,#22989,#22990,#22991,#22992,
#22993,#22994,#22995,#22996,#22997,#22998,#22999,#23000,#23001,#23002,#23003,
#23004,#23005,#23006,#23007,#23008,#23009,#23010,#23011,#23012),
 .UNSPECIFIED.,.F.,.F.,(4,2,2,2,2,2,2,2,2,2,2,2,2,2,2,2,2,2,2,2,2,2,2,2,
2,2,2,2,2,2,2,2,2,2,2,2,2,2,2,2,2,2,2,2,2,2,2,2,2,2,4),(-0.662395452864075,
-0.636565501350124,-0.590829186366297,-0.589512179980496,-0.587975443379499,
-0.585595470404861,-0.583104391398326,-0.580517051134528,-0.579581367318058,
-0.579037786371118,-0.578528599275995,-0.577818467473817,-0.57705282609667,
-0.573316651020191,-0.547688846920168,-0.504753401896079,-0.425388452164051,
-0.42070173659393,-0.418843089666003,-0.417830834810713,-0.416825732222374,
-0.41560047040439,-0.414298672346237,-0.40867105374896,-0.39985425249306,
-0.390990068151443,-0.350308828085196,-0.319371310780197,-0.261149804359824,
-0.257753554155548,-0.256709046194757,-0.256143601808686,-0.25563892205914,
-0.254971287059037,-0.254264803884776,-0.25316399171694,-0.239472971966821,
-0.209699904381192,-0.19815665668234,-0.1857773545203,-0.102943180665461,
-0.0975759915845706,-0.0957931285325462,-0.0947961661521012,-0.0937987644111212,
-0.0925503530051014,-0.0912164737157821,-0.0890874625231243,-0.0849683350027143,
-0.0749314486993903,-0.000961829325271721),.UNSPECIFIED.);
#135=B_SPLINE_CURVE_WITH_KNOTS('',3,(#23013,#23014,#23015,#23016,#23017,
#23018,#23019,#23020,#23021,#23022,#23023,#23024,#23025,#23026,#23027,#23028,
#23029,#23030,#23031,#23032,#23033,#23034,#23035,#23036,#23037,#23038,#23039,
#23040,#23041,#23042,#23043,#23044,#23045,#23046,#23047,#23048,#23049,#23050,
#23051,#23052,#23053,#23054,#23055,#23056,#23057,#23058,#23059,#23060,#23061,
#23062,#23063,#23064,#23065,#23066,#23067,#23068,#23069,#23070,#23071,#23072,
#23073,#23074,#23075,#23076,#23077,#23078,#23079,#23080,#23081,#23082,#23083,
#23084,#23085,#23086,#23087,#23088,#23089,#23090,#23091,#23092,#23093,#23094,
#23095,#23096,#23097,#23098,#23099,#23100,#23101,#23102,#23103,#23104,#23105,
#23106,#23107,#23108,#23109,#23110,#23111,#23112,#23113,#23114,#23115,#23116,
#23117,#23118,#23119,#23120,#23121,#23122,#23123,#23124,#23125,#23126,#23127,
#23128,#23129,#23130,#23131,#23132,#23133,#23134,#23135,#23136,#23137,#23138,
#23139,#23140,#23141,#23142,#23143,#23144,#23145,#23146,#23147,#23148,#23149,
#23150,#23151,#23152,#23153,#23154,#23155,#23156,#23157,#23158,#23159,#23160,
#23161,#23162,#23163,#23164,#23165,#23166,#23167,#23168,#23169,#23170,#23171,
#23172,#23173,#23174,#23175,#23176,#23177,#23178,#23179,#23180,#23181,#23182,
#23183,#23184,#23185,#23186,#23187,#23188,#23189,#23190,#23191,#23192,#23193,
#23194,#23195,#23196,#23197,#23198,#23199,#23200,#23201,#23202,#23203,#23204,
#23205,#23206,#23207,#23208,#23209,#23210,#23211,#23212,#23213,#23214,#23215,
#23216,#23217,#23218),.UNSPECIFIED.,.F.,.F.,(4,2,2,2,2,2,2,2,2,2,2,2,2,
2,2,2,2,2,2,2,2,2,2,2,2,2,2,2,2,2,2,2,2,2,2,2,2,2,2,2,2,2,2,2,2,2,2,2,2,
2,2,2,2,2,2,2,2,2,2,2,2,2,2,2,2,2,2,2,2,2,2,2,2,2,2,2,2,2,2,2,2,2,2,2,2,
2,2,2,2,2,2,2,2,2,2,2,2,2,2,2,2,2,4),(-4.06006530123386,-3.99593991466936,
-3.99430387186957,-3.9933769546758,-3.99274336851389,-3.99212731294241,
-3.9915604833862,-3.99082368469873,-3.98922136288891,-3.9771514282463,-3.97510372004162,
-3.97461684272393,-3.97374861055896,-3.96784184438647,-3.95507851342347,
-3.92543386522881,-3.91690570768221,-3.90966437886953,-3.89489898230916,
-3.85256905838493,-3.83588564108468,-3.83381613980117,-3.83250748149031,
-3.83127738652211,-3.83036911203196,-3.82938495512678,-3.82796266426522,
-3.82395043408515,-3.82266924319363,-3.74316329855756,-3.72031522011211,
-3.69481234516365,-3.67906531570999,-3.67407311879412,-3.67093248230224,
-3.67020563918313,-3.66952348234982,-3.66896871779134,-3.66839881246668,
-3.66733142307643,-3.6637395159226,-3.60549518398974,-3.55950594500283,
-3.55189279906574,-3.51687800481418,-3.51100915382049,-3.50969145809721,
-3.50845483010772,-3.50754577578874,-3.50656467935198,-3.50485977975429,
-3.50004614720885,-3.42544685303681,-3.37701913855712,-3.35727362876052,
-3.34873949569421,-3.34740795648504,-3.34671162303826,-3.34615080630097,
-3.34558777111391,-3.34455452491803,-3.34124837980412,-3.28905379980431,
-3.22614436275744,-3.20153367704954,-3.18913095355246,-3.18682598251588,
-3.18559021312565,-3.18468124314283,-3.18369971007095,-3.18228699071446,
-3.178338898215,-3.11411446234708,-3.06060876373378,-3.03538624870023,-3.0259492755416,
-3.02458443852319,-3.02388107681627,-3.02337298006682,-3.02282691301624,
-3.02187801821909,-3.01920017826794,-2.97745115374412,-2.91086901244872,
-2.87166941637895,-2.86539241627176,-2.86355689715973,-2.86243762648458,
-2.86142708543733,-2.86013658978368,-2.85750224874746,-2.84138979380937,
-2.83808653633522,-2.81844691435209,-2.75778430521744,-2.70557692191206,
-2.70241421602068,-2.70144053860748,-2.7008239226418,-2.70025717708969,
-2.69952130947825,-2.6979242304867,-2.69214944809879),.UNSPECIFIED.);
#136=B_SPLINE_CURVE_WITH_KNOTS('',3,(#23224,#23225,#23226,#23227,#23228,
#23229,#23230,#23231,#23232,#23233,#23234,#23235,#23236,#23237,#23238,#23239,
#23240,#23241,#23242,#23243,#23244,#23245,#23246,#23247,#23248,#23249,#23250,
#23251,#23252,#23253,#23254,#23255,#23256,#23257,#23258,#23259,#23260,#23261,
#23262,#23263,#23264,#23265,#23266,#23267,#23268,#23269,#23270,#23271,#23272,
#23273,#23274,#23275,#23276,#23277,#23278,#23279,#23280,#23281,#23282,#23283,
#23284,#23285,#23286,#23287,#23288,#23289,#23290,#23291,#23292,#23293,#23294,
#23295,#23296,#23297,#23298,#23299,#23300,#23301,#23302,#23303,#23304,#23305,
#23306,#23307,#23308,#23309,#23310,#23311,#23312,#23313,#23314,#23315,#23316,
#23317,#23318,#23319,#23320,#23321,#23322,#23323,#23324,#23325,#23326,#23327,
#23328,#23329,#23330,#23331,#23332,#23333,#23334,#23335,#23336,#23337,#23338,
#23339,#23340,#23341,#23342,#23343,#23344,#23345,#23346,#23347,#23348,#23349,
#23350,#23351,#23352,#23353,#23354,#23355,#23356,#23357,#23358,#23359,#23360,
#23361,#23362,#23363,#23364,#23365,#23366,#23367,#23368,#23369,#23370,#23371,
#23372,#23373,#23374,#23375,#23376,#23377,#23378,#23379,#23380,#23381,#23382,
#23383,#23384,#23385,#23386,#23387,#23388,#23389,#23390,#23391,#23392,#23393,
#23394,#23395,#23396,#23397,#23398,#23399,#23400,#23401,#23402,#23403,#23404,
#23405,#23406,#23407,#23408,#23409,#23410,#23411,#23412,#23413,#23414,#23415,
#23416,#23417,#23418,#23419,#23420,#23421,#23422,#23423,#23424,#23425,#23426,
#23427,#23428,#23429,#23430,#23431,#23432,#23433,#23434,#23435,#23436,#23437),
 .UNSPECIFIED.,.F.,.F.,(4,2,2,2,2,2,2,2,2,2,2,2,2,2,2,2,2,2,2,2,2,2,2,2,
2,2,2,2,2,2,2,2,2,2,2,2,2,2,2,2,2,2,2,2,2,2,2,2,2,2,2,2,2,2,2,2,2,2,2,2,
2,2,2,2,2,2,2,2,2,2,2,2,2,2,2,2,2,2,2,2,2,2,2,2,2,2,2,2,2,2,2,2,2,2,2,2,
2,2,2,2,2,2,2,2,2,2,4),(-1.37024023670309,-1.36885167238846,-1.33918962176659,
-1.33638108529293,-1.33502146057737,-1.3340544383004,-1.33305966031228,
-1.33177427202646,-1.3303641635137,-1.3280530028917,-1.32344559768138,-1.27628892863603,
-1.17911015497803,-1.17434917215125,-1.17326514267846,-1.1725643668986,
-1.17200309625918,-1.17135908291938,-1.17024336810341,-1.16562014005557,
-1.12657943799402,-1.02060934691787,-1.0140511329824,-1.01212151688076,
-1.01098112950292,-1.00998834902539,-1.00876456961566,-1.00642464706627,
-1.00347844038503,-0.997080642333151,-0.977435942618436,-0.927270753068591,
-0.886221429308439,-0.873693875777526,-0.867040205987696,-0.852105177954858,
-0.850427825445548,-0.849733316503579,-0.849159091260957,-0.84856913663225,
-0.847696981178548,-0.84533302716629,-0.787568498767643,-0.711474735972392,
-0.708321437405196,-0.692358461587232,-0.689731838698381,-0.688442875037336,
-0.687432500458816,-0.686334866794259,-0.684559153910981,-0.682455766303399,
-0.678403807561126,-0.668585031234653,-0.635050126915235,-0.532622904138751,
-0.531763392050551,-0.528038059754367,-0.526955284617288,-0.526382182847298,
-0.525878091846954,-0.525221580052896,-0.524049310450672,-0.518660244991595,
-0.508455649384645,-0.479514883812686,-0.470545709694636,-0.463050638639729,
-0.456597765866444,-0.450942365951417,-0.399256529645745,-0.370093641699301,
-0.367296592158299,-0.365939646120318,-0.364973218567505,-0.36400101406144,
-0.363017270793776,-0.360863175342903,-0.350312791231922,-0.330173896685716,
-0.309272020054442,-0.215129716287474,-0.213784119410423,-0.212208998046509,
-0.209582714806551,-0.209190457159851,-0.205121174966834,-0.204014264593347,
-0.203365635890036,-0.20280470427498,-0.202109923132213,-0.200759446328427,
-0.191852023116426,-0.170477733469139,-0.0836889393789725,-0.0780371380388596,
-0.0704778394857391,-0.0674444858369929,-0.046585140615017,-0.0440273660684284,
-0.0427303186481333,-0.0417796549327277,-0.0408180730834325,-0.0398220982889161,
-0.0385198626423396,-0.0364660321025074,-0.000960727209027502),
 .UNSPECIFIED.);
#137=B_SPLINE_CURVE_WITH_KNOTS('',3,(#23438,#23439,#23440,#23441,#23442,
#23443,#23444,#23445,#23446,#23447,#23448,#23449,#23450,#23451,#23452,#23453,
#23454,#23455,#23456,#23457,#23458,#23459,#23460,#23461,#23462,#23463,#23464,
#23465,#23466,#23467,#23468,#23469,#23470,#23471,#23472,#23473,#23474,#23475,
#23476,#23477,#23478,#23479,#23480,#23481,#23482,#23483,#23484,#23485,#23486,
#23487,#23488,#23489,#23490,#23491,#23492,#23493,#23494,#23495,#23496,#23497,
#23498,#23499,#23500,#23501,#23502,#23503,#23504,#23505,#23506,#23507,#23508,
#23509,#23510,#23511,#23512,#23513,#23514,#23515,#23516,#23517,#23518,#23519,
#23520,#23521,#23522,#23523,#23524,#23525,#23526,#23527,#23528,#23529),
 .UNSPECIFIED.,.F.,.F.,(4,2,2,2,2,2,2,2,2,2,2,2,2,2,2,2,2,2,2,2,2,2,2,2,
2,2,2,2,2,2,2,2,2,2,2,2,2,2,2,2,2,2,2,2,2,4),(-4.06085215427619,-3.96661118569572,
-3.94505040122191,-3.94164875373561,-3.94064622429485,-3.94002742739455,
-3.93946101715168,-3.93872877242596,-3.93715189450824,-3.92576039072985,
-3.92461321105174,-3.881110884479,-3.82992662093111,-3.81419971635615,-3.79323860015488,
-3.7823613668101,-3.78018703772864,-3.779201058095,-3.77823068752792,-3.77726700444125,
-3.77592080727929,-3.77316795992076,-3.74580419666669,-3.70680899915316,
-3.67860169565895,-3.6237167615223,-3.61893501839857,-3.61780662874518,
-3.61715969714152,-3.6165985625392,-3.61590139435704,-3.61482927084666,
-3.61003056804398,-3.51717975406838,-3.47935504024415,-3.46641744885073,
-3.46144162184887,-3.45899543550808,-3.45698860284708,-3.45583645997346,
-3.45492707099901,-3.45390846893587,-3.45201849694706,-3.44580458898125,
-3.4444266686727,-3.39977149278874),.UNSPECIFIED.);
#138=B_SPLINE_CURVE_WITH_KNOTS('',3,(#23530,#23531,#23532,#23533,#23534,
#23535,#23536,#23537,#23538,#23539,#23540,#23541,#23542,#23543,#23544,#23545,
#23546,#23547,#23548,#23549,#23550,#23551,#23552,#23553,#23554,#23555,#23556,
#23557,#23558,#23559,#23560,#23561,#23562,#23563,#23564,#23565,#23566,#23567,
#23568,#23569,#23570,#23571,#23572,#23573,#23574,#23575,#23576,#23577,#23578,
#23579,#23580,#23581,#23582,#23583,#23584,#23585,#23586,#23587,#23588,#23589,
#23590,#23591,#23592,#23593,#23594,#23595,#23596,#23597,#23598,#23599,#23600,
#23601,#23602,#23603,#23604,#23605,#23606,#23607,#23608,#23609,#23610,#23611,
#23612,#23613,#23614,#23615,#23616,#23617,#23618,#23619,#23620,#23621,#23622,
#23623,#23624,#23625,#23626,#23627,#23628,#23629,#23630,#23631,#23632,#23633,
#23634,#23635,#23636,#23637,#23638,#23639,#23640,#23641,#23642,#23643,#23644,
#23645,#23646,#23647,#23648,#23649,#23650,#23651,#23652,#23653,#23654,#23655,
#23656,#23657,#23658,#23659,#23660,#23661,#23662,#23663,#23664,#23665,#23666,
#23667,#23668,#23669,#23670,#23671,#23672,#23673,#23674,#23675,#23676,#23677,
#23678,#23679,#23680,#23681,#23682,#23683,#23684,#23685,#23686,#23687,#23688,
#23689,#23690,#23691,#23692,#23693,#23694,#23695,#23696,#23697,#23698,#23699,
#23700,#23701,#23702,#23703,#23704,#23705,#23706,#23707,#23708,#23709,#23710,
#23711,#23712,#23713,#23714,#23715,#23716,#23717,#23718,#23719,#23720,#23721,
#23722,#23723,#23724,#23725,#23726,#23727,#23728,#23729,#23730,#23731,#23732,
#23733,#23734,#23735,#23736,#23737,#23738,#23739,#23740,#23741,#23742,#23743,
#23744,#23745,#23746,#23747,#23748,#23749,#23750,#23751,#23752,#23753,#23754,
#23755,#23756,#23757,#23758,#23759,#23760,#23761,#23762,#23763,#23764,#23765,
#23766,#23767,#23768,#23769,#23770,#23771,#23772,#23773,#23774,#23775,#23776,
#23777,#23778,#23779,#23780,#23781,#23782,#23783,#23784,#23785,#23786,#23787,
#23788,#23789,#23790,#23791,#23792,#23793,#23794,#23795,#23796,#23797,#23798,
#23799,#23800,#23801,#23802,#23803,#23804,#23805,#23806,#23807,#23808,#23809,
#23810,#23811,#23812,#23813,#23814,#23815,#23816,#23817,#23818,#23819,#23820,
#23821,#23822,#23823),.UNSPECIFIED.,.F.,.F.,(4,2,2,2,2,2,2,2,2,2,2,2,2,
2,2,2,2,2,2,2,2,2,2,2,2,2,2,2,2,2,2,2,2,2,2,2,2,2,2,2,2,2,2,2,2,2,2,2,2,
2,2,2,2,2,2,2,2,2,2,2,2,2,2,2,2,2,2,2,2,2,2,2,2,2,2,2,2,2,2,2,2,2,2,2,2,
2,2,2,2,2,2,2,2,2,2,2,2,2,2,2,2,2,2,2,2,2,2,2,2,2,2,2,2,2,2,2,2,2,2,2,2,
2,2,2,2,2,2,2,2,2,2,2,2,2,2,2,2,2,2,2,2,2,2,2,2,2,4),(-2.69214944809879,
-2.68599658157334,-2.67164723329084,-2.65509714678797,-2.62302784577316,
-2.57819043594351,-2.55508852161463,-2.54343864667162,-2.54116300941676,
-2.53993686756713,-2.5389320190232,-2.5379208437841,-2.536066545589,-2.53014312996771,
-2.52835564554769,-2.52586301442259,-2.52446243206274,-2.52344138183711,
-2.52302472034248,-2.43489025317887,-2.38268558995137,-2.37952643746347,
-2.37855319968038,-2.37793656392635,-2.37736971714667,-2.37663360430841,
-2.37503554803698,-2.36308644350046,-2.36087945763509,-2.36049387330735,
-2.32702594666857,-2.30391962788928,-2.25052638850229,-2.23391651921538,
-2.22054467523627,-2.21823333148908,-2.21700936486661,-2.21600450708303,
-2.21499180532168,-2.21313034550096,-2.20715001965889,-2.10547356610973,
-2.08147726364995,-2.05996426419309,-2.05656741720115,-2.05556550413876,
-2.05494690653567,-2.0543805526434,-2.05364820869943,-2.0520704543158,-2.04065253546098,
-2.03952931049749,-2.03914938575955,-2.03631552362315,-2.0352630986408,
-2.03410163508923,-2.03130204021125,-2.00261033368606,-1.93396926714356,
-1.89894135520261,-1.89575631506156,-1.89446685351192,-1.89351816229621,
-1.89249242633389,-1.89110197661171,-1.88794272980815,-1.84713509200039,
-1.78939754286815,-1.74366517471266,-1.74246691729439,-1.74094611924842,
-1.73823781239039,-1.73391081223565,-1.7327781881313,-1.73212361544069,
-1.73156317725347,-1.73087607758004,-1.72956203351273,-1.72155551617218,
-1.71106989723019,-1.68755219755491,-1.57975761495329,-1.57361537612516,
-1.57173429009616,-1.57071765644577,-1.5697131311958,-1.56852014575054,
-1.56632053594682,-1.5635903138388,-1.50786062815447,-1.43010552010928,
-1.42871949470108,-1.42786781760932,-1.42684354708768,-1.41167903906937,
-1.41014209882668,-1.4093919523983,-1.40885551810102,-1.40834350163467,
-1.40761425417709,-1.40609313506553,-1.39049976505409,-1.3732305669527,
-1.25634517856986,-1.25038514061555,-1.24852638739162,-1.24751435322766,
-1.24650964645382,-1.24530990826964,-1.24308525745988,-1.24031256631594,
-1.17480270146845,-1.09798392690746,-1.09545748565058,-1.08800232770736,
-1.08675514599148,-1.08601284293542,-1.08544506075773,-1.08483132089616,
-1.08385070524348,-1.08064490803196,-1.03238043366701,-0.940483867016562,
-0.939790740022388,-0.938376955615533,-0.934889008839562,-0.93347217413441,
-0.927396635145153,-0.92552378011985,-0.924508907565407,-0.923504432870422,
-0.922309172581548,-0.92010157690178,-0.917357183811406,-0.911542850101569,
-0.895585524246291,-0.878811346126955,-0.775268882508638,-0.765126928909412,
-0.763603068084822,-0.762873291272256,-0.762309023457881,-0.761682957156301,
-0.76064752433179,-0.756925759970814,-0.668028289659514,-0.661829640843947),
 .UNSPECIFIED.);
#139=B_SPLINE_CURVE_WITH_KNOTS('',3,(#23828,#23829,#23830,#23831,#23832,
#23833,#23834,#23835,#23836,#23837,#23838,#23839,#23840,#23841,#23842,#23843,
#23844,#23845,#23846,#23847,#23848,#23849,#23850,#23851,#23852,#23853,#23854,
#23855,#23856,#23857,#23858,#23859,#23860,#23861,#23862,#23863,#23864,#23865,
#23866,#23867,#23868,#23869,#23870,#23871,#23872,#23873,#23874,#23875,#23876,
#23877,#23878,#23879,#23880,#23881,#23882,#23883,#23884,#23885,#23886,#23887,
#23888,#23889,#23890,#23891,#23892,#23893,#23894,#23895,#23896,#23897,#23898,
#23899,#23900,#23901,#23902,#23903,#23904,#23905,#23906,#23907,#23908,#23909,
#23910,#23911,#23912,#23913,#23914,#23915,#23916,#23917,#23918,#23919,#23920,
#23921,#23922,#23923,#23924,#23925,#23926,#23927,#23928,#23929,#23930,#23931,
#23932,#23933,#23934,#23935,#23936,#23937,#23938,#23939,#23940,#23941,#23942,
#23943,#23944,#23945,#23946,#23947,#23948,#23949,#23950,#23951,#23952,#23953,
#23954,#23955,#23956,#23957,#23958,#23959,#23960,#23961,#23962,#23963,#23964,
#23965,#23966,#23967,#23968,#23969,#23970,#23971,#23972,#23973,#23974,#23975,
#23976,#23977,#23978,#23979,#23980,#23981,#23982,#23983,#23984,#23985,#23986,
#23987,#23988,#23989,#23990,#23991,#23992,#23993,#23994,#23995,#23996,#23997,
#23998,#23999,#24000,#24001,#24002,#24003,#24004,#24005,#24006,#24007,#24008,
#24009,#24010,#24011,#24012,#24013,#24014,#24015,#24016,#24017,#24018,#24019,
#24020,#24021,#24022,#24023,#24024,#24025,#24026,#24027,#24028,#24029,#24030,
#24031,#24032,#24033,#24034,#24035,#24036,#24037,#24038,#24039,#24040,#24041,
#24042,#24043,#24044,#24045,#24046,#24047,#24048,#24049,#24050,#24051,#24052,
#24053,#24054,#24055,#24056,#24057,#24058,#24059,#24060,#24061,#24062,#24063,
#24064,#24065,#24066,#24067,#24068,#24069,#24070,#24071,#24072,#24073,#24074,
#24075,#24076,#24077,#24078,#24079,#24080,#24081,#24082,#24083,#24084,#24085,
#24086,#24087,#24088,#24089,#24090,#24091,#24092,#24093,#24094,#24095,#24096,
#24097,#24098,#24099,#24100,#24101,#24102,#24103),.UNSPECIFIED.,.F.,.F.,
(4,2,2,2,2,2,2,2,2,2,2,2,2,2,2,2,2,2,2,2,2,2,2,2,2,2,2,2,2,2,2,2,2,2,2,
2,2,2,2,2,2,2,2,2,2,2,2,2,2,2,2,2,2,2,2,2,2,2,2,2,2,2,2,2,2,2,2,2,2,2,2,
2,2,2,2,2,2,2,2,2,2,2,2,2,2,2,2,2,2,2,2,2,2,2,2,2,2,2,2,2,2,2,2,2,2,2,2,
2,2,2,2,2,2,2,2,2,2,2,2,2,2,2,2,2,2,2,2,2,2,2,2,2,2,2,2,2,2,4),(-3.40024812751307,
-3.37021916983221,-3.32505019996527,-3.29549526830059,-3.27634593457388,
-3.27382180366001,-3.27255376852381,-3.27164074029554,-3.27067323796775,
-3.26931121453177,-3.26649211847317,-3.25891046188894,-3.25709606806721,
-3.25503353230855,-3.25458896974936,-3.25267312412952,-3.24984890603887,
-3.24865288393459,-3.24708911667439,-3.23994482018547,-3.15121175955301,
-3.12608702916532,-3.1172488270471,-3.1140601592006,-3.11255553194174,-3.11168174036197,
-3.11090401195614,-3.11033974796076,-3.10981351113754,-3.10910193962852,
-3.10771729758783,-3.09724890235979,-3.03503339651356,-2.98935503809951,
-2.95761659599998,-2.9520834524647,-2.9503486946786,-2.94925202831025,-2.9482353774998,
-2.94692141582952,-2.9440941679695,-2.92357931905998,-2.91988743292052,
-2.84174555527698,-2.79252922098714,-2.79036968852979,-2.78923835395744,
-2.78851916476895,-2.7878519530383,-2.7873038773602,-2.78673510546515,-2.78567331828929,
-2.78212950731031,-2.78092411161475,-2.7784739014207,-2.77692093140824,
-2.77549266362795,-2.68198167080393,-2.64592939769034,-2.63034070536811,
-2.62793597241531,-2.62669255959398,-2.62568678346382,-2.62468565083225,
-2.62288053256954,-2.61734151151723,-2.52610469716422,-2.46866414594993,
-2.4669309876275,-2.46596527014986,-2.46531553269414,-2.46469783232534,
-2.46417692554638,-2.46347710868523,-2.46239584831783,-2.45747895060558,
-2.36318259380599,-2.34220468439246,-2.32268794950534,-2.30730096877307,
-2.30490399878233,-2.30366218180784,-2.30265648912325,-2.30165444058315,
-2.29984489728978,-2.29427231313607,-2.17518737874915,-2.15286470772111,
-2.14372993825883,-2.14237127619577,-2.1416748952449,-2.14111398449238,
-2.14046685084458,-2.13936592841587,-2.13535293397075,-2.13488836811322,
-2.03154911500209,-1.98560467267569,-1.98222998666102,-1.98090832922995,
-1.97995145026512,-1.97893140643873,-1.97757380041888,-1.97459247319502,
-1.9168325927431,-1.83074030828404,-1.82084482997164,-1.81933216524787,
-1.81860461207888,-1.81804064490914,-1.81741342729343,-1.81637276606867,
-1.81259753465822,-1.72383023213061,-1.66332207640873,-1.65938351405851,
-1.65797215662046,-1.6569909468046,-1.65600096995921,-1.65475202895635,
-1.65339223458445,-1.65120127405137,-1.64691717922249,-1.6056349906904,
-1.55463124828268,-1.51653942581854,-1.51528751052423,-1.51211488756194,
-1.51021841535422,-1.49802245798605,-1.49643573940522,-1.4956904168319,
-1.49512215526703,-1.49450975473211,-1.49353510962024,-1.49038140500459,
-1.4382436320602,-1.37024023670309),.UNSPECIFIED.);
#140=B_SPLINE_CURVE_WITH_KNOTS('',3,(#24105,#24106,#24107,#24108,#24109,
#24110,#24111,#24112,#24113,#24114,#24115,#24116,#24117,#24118,#24119,#24120,
#24121,#24122,#24123,#24124,#24125,#24126,#24127,#24128,#24129,#24130,#24131,
#24132,#24133,#24134,#24135,#24136,#24137,#24138,#24139,#24140,#24141,#24142,
#24143,#24144,#24145,#24146,#24147,#24148,#24149,#24150,#24151,#24152,#24153,
#24154,#24155,#24156,#24157,#24158,#24159,#24160,#24161,#24162,#24163,#24164,
#24165,#24166,#24167,#24168,#24169,#24170,#24171,#24172,#24173,#24174,#24175,
#24176,#24177,#24178,#24179,#24180,#24181,#24182,#24183,#24184,#24185,#24186,
#24187,#24188,#24189,#24190,#24191,#24192,#24193,#24194,#24195,#24196),
 .UNSPECIFIED.,.F.,.F.,(4,2,2,2,2,2,2,2,2,2,2,2,2,2,2,2,2,2,2,2,2,2,2,2,
2,2,2,2,2,2,2,2,2,2,2,2,2,2,2,2,2,2,2,2,2,4),(-0.661829640843947,-0.612715495677179,
-0.609522028636577,-0.604119517181893,-0.602332136058833,-0.601334391212832,
-0.600339656054466,-0.599119487924847,-0.596806779067315,-0.593896446576099,
-0.587603514970783,-0.569857605629294,-0.535118957266086,-0.468698656885868,
-0.442776896139604,-0.44086781458186,-0.440126211952284,-0.439592078982841,
-0.439021836344277,-0.438251521035448,-0.43651283520404,-0.380557851560157,
-0.352976448378946,-0.317068882730308,-0.305814394758379,-0.303764843847665,
-0.283059322801507,-0.280223842026451,-0.278908057692136,-0.277890852002289,
-0.276949508423118,-0.275874397196253,-0.272880906583698,-0.245790281652857,
-0.226149685341142,-0.122939428242058,-0.122348526875143,-0.118428655112071,
-0.117337330991179,-0.116692336686235,-0.116131046265131,-0.115431322461575,
-0.114057065785592,-0.104489937707715,-0.0741047509759709,-0.000962458815746768),
 .UNSPECIFIED.);
#141=B_SPLINE_CURVE_WITH_KNOTS('',3,(#24197,#24198,#24199,#24200,#24201,
#24202,#24203,#24204,#24205,#24206,#24207,#24208,#24209,#24210,#24211,#24212,
#24213,#24214,#24215,#24216,#24217,#24218,#24219,#24220,#24221,#24222,#24223,
#24224,#24225,#24226,#24227,#24228,#24229,#24230,#24231,#24232,#24233,#24234,
#24235,#24236,#24237,#24238,#24239,#24240,#24241,#24242,#24243,#24244,#24245,
#24246,#24247,#24248,#24249,#24250,#24251,#24252,#24253,#24254,#24255,#24256,
#24257,#24258,#24259,#24260,#24261,#24262,#24263,#24264,#24265,#24266,#24267,
#24268,#24269,#24270,#24271,#24272,#24273,#24274,#24275,#24276,#24277,#24278,
#24279,#24280,#24281,#24282,#24283,#24284,#24285,#24286,#24287,#24288,#24289,
#24290,#24291,#24292,#24293,#24294,#24295,#24296,#24297,#24298,#24299,#24300,
#24301,#24302,#24303,#24304,#24305,#24306,#24307,#24308,#24309,#24310,#24311,
#24312,#24313,#24314,#24315,#24316,#24317,#24318,#24319,#24320,#24321,#24322,
#24323,#24324,#24325,#24326,#24327,#24328,#24329,#24330,#24331,#24332,#24333,
#24334,#24335,#24336,#24337,#24338,#24339,#24340,#24341,#24342,#24343,#24344,
#24345,#24346,#24347,#24348,#24349,#24350,#24351,#24352,#24353,#24354,#24355,
#24356,#24357,#24358,#24359,#24360,#24361,#24362,#24363,#24364,#24365,#24366,
#24367,#24368,#24369,#24370,#24371,#24372,#24373,#24374,#24375,#24376,#24377,
#24378,#24379,#24380,#24381,#24382,#24383,#24384,#24385,#24386,#24387,#24388),
 .UNSPECIFIED.,.F.,.F.,(4,2,2,2,2,2,2,2,2,2,2,2,2,2,2,2,2,2,2,2,2,2,2,2,
2,2,2,2,2,2,2,2,2,2,2,2,2,2,2,2,2,2,2,2,2,2,2,2,2,2,2,2,2,2,2,2,2,2,2,2,
2,2,2,2,2,2,2,2,2,2,2,2,2,2,2,2,2,2,2,2,2,2,2,2,2,2,2,2,2,2,2,2,2,2,2,4),
(-4.06434128415624,-4.0235371652522,-4.02147772617206,-4.0201729447231,
-4.01917586288143,-4.0182144098793,-4.01726414507108,-4.01596962822361,
-4.01275735295853,-3.97648937458706,-3.97075261283844,-3.88496254663774,
-3.86338044728011,-3.85870753133827,-3.8575873851824,-3.85694213702144,
-3.85638060100868,-3.85568053937851,-3.85459955003203,-3.84982856687511,
-3.75265760584019,-3.72967907984624,-3.70953059977957,-3.69897396417434,
-3.69681873467038,-3.69583448739759,-3.6948617922275,-3.69389487008252,
-3.692537242744,-3.68973882301341,-3.66056268890683,-3.62783061094541,-3.53916688352163,
-3.53530040134573,-3.53425040860409,-3.53362080452173,-3.53311572485325,
-3.53242104173421,-3.53135736474281,-3.52666512443278,-3.52470534154804,
-3.52268180933885,-3.52177204832499,-3.44482679401666,-3.40988559860286,
-3.38736966622947,-3.3798251942801,-3.37649407866723,-3.37390737872275,
-3.37263117305147,-3.37165782117644,-3.37069000434681,-3.36932931693261,
-3.36651875320827,-3.33684487209056,-3.24939477818891,-3.23528733525964,
-3.21987123318882,-3.2125110214233,-3.21122568242145,-3.21054439387533,
-3.20998911961032,-3.2094176112918,-3.2083440938561,-3.20470484662442,-3.20370616047174,
-3.12780535613794,-3.06003893212251,-3.05485716287473,-3.05233629789206,
-3.05027706748941,-3.04911388927411,-3.04820856951106,-3.04719831149225,
-3.04535136529604,-3.03949502681541,-2.94860271366907,-2.89370248792994,
-2.88891342821127,-2.88778405825408,-2.88713669242884,-2.88657525872605,
-2.88587781754436,-2.88480545482924,-2.88000857223905,-2.79325492436669,
-2.75746353606728,-2.73286597244475,-2.72971425450522,-2.72724047666725,
-2.72598815011584,-2.72500628237635,-2.72402647278784,-2.7226221422139,
-2.71873495995085,-2.69413699669498),.UNSPECIFIED.);
#142=B_SPLINE_CURVE_WITH_KNOTS('',3,(#24394,#24395,#24396,#24397,#24398,
#24399,#24400,#24401,#24402,#24403,#24404,#24405,#24406,#24407,#24408,#24409,
#24410,#24411,#24412,#24413,#24414,#24415,#24416,#24417,#24418,#24419,#24420,
#24421,#24422,#24423,#24424,#24425,#24426,#24427,#24428,#24429,#24430,#24431,
#24432,#24433,#24434,#24435,#24436,#24437,#24438,#24439,#24440,#24441,#24442,
#24443,#24444,#24445,#24446,#24447,#24448,#24449,#24450,#24451,#24452,#24453,
#24454,#24455,#24456,#24457,#24458,#24459,#24460,#24461,#24462,#24463,#24464,
#24465,#24466,#24467,#24468,#24469,#24470,#24471,#24472,#24473,#24474,#24475,
#24476,#24477,#24478,#24479,#24480,#24481,#24482,#24483,#24484,#24485,#24486,
#24487,#24488,#24489,#24490,#24491,#24492,#24493,#24494,#24495,#24496,#24497,
#24498,#24499,#24500,#24501,#24502,#24503,#24504,#24505,#24506,#24507,#24508,
#24509,#24510,#24511,#24512,#24513,#24514,#24515,#24516,#24517,#24518,#24519,
#24520,#24521,#24522,#24523,#24524,#24525,#24526,#24527,#24528,#24529,#24530,
#24531,#24532,#24533,#24534,#24535,#24536,#24537,#24538,#24539,#24540,#24541,
#24542,#24543,#24544,#24545,#24546,#24547,#24548,#24549,#24550,#24551,#24552,
#24553,#24554,#24555,#24556,#24557,#24558,#24559,#24560,#24561,#24562,#24563,
#24564,#24565,#24566,#24567,#24568,#24569,#24570,#24571,#24572,#24573,#24574,
#24575,#24576,#24577,#24578,#24579,#24580,#24581,#24582,#24583,#24584,#24585,
#24586,#24587,#24588,#24589,#24590,#24591,#24592,#24593,#24594,#24595,#24596,
#24597,#24598,#24599,#24600,#24601,#24602,#24603,#24604,#24605,#24606,#24607,
#24608,#24609,#24610,#24611,#24612,#24613),.UNSPECIFIED.,.F.,.F.,(4,2,2,
2,2,2,2,2,2,2,2,2,2,2,2,2,2,2,2,2,2,2,2,2,2,2,2,2,2,2,2,2,2,2,2,2,2,2,2,
2,2,2,2,2,2,2,2,2,2,2,2,2,2,2,2,2,2,2,2,2,2,2,2,2,2,2,2,2,2,2,2,2,2,2,2,
2,2,2,2,2,2,2,2,2,2,2,2,2,2,2,2,2,2,2,2,2,2,2,2,2,2,2,2,2,2,2,2,2,2,4),
(-1.37029241472368,-1.34852183284429,-1.32293951683633,-1.32190342284898,
-1.32024765934368,-1.31568780184551,-1.31290518130904,-1.31194094441941,
-1.31139159029801,-1.31083876931964,-1.31013340499299,-1.30936095701649,
-1.30810273240195,-1.30560447221522,-1.21681269106214,-1.15605542670002,
-1.15226951861025,-1.15088107844413,-1.14990591692488,-1.1489945323053,
-1.14774264003818,-1.14529965598708,-1.12871102886337,-1.08886453232611,
-1.02576386691761,-0.991713875009911,-0.989560785485333,-0.988780806232009,
-0.988236141085219,-0.987681891714349,-0.987015362115503,-0.986251110731604,
-0.985012511128443,-0.982567395750004,-0.976411545159215,-0.953528875623381,
-0.835360269432715,-0.829606039922391,-0.827772662119502,-0.826765541908211,
-0.825760001368634,-0.824526100042465,-0.822168279555364,-0.807758621240536,
-0.776358983332107,-0.763557029442697,-0.752734994118637,-0.671336471262862,
-0.670352264020728,-0.666707046606074,-0.665633237725656,-0.665061881665321,
-0.664512611575234,-0.663901279564926,-0.663207842460111,-0.662138098892671,
-0.660139713329433,-0.655456388248882,-0.640646275202323,-0.627648913650835,
-0.512387104486719,-0.50642894179736,-0.504570223350185,-0.503558085194288,
-0.502553197247076,-0.50132834042526,-0.499012752832494,-0.4855490784644,
-0.469710938186427,-0.437836036271502,-0.4285707453202,-0.420841685803779,
-0.414214832438632,-0.408426633596053,-0.390147630057129,-0.373870415288781,
-0.345056568661516,-0.343102105789311,-0.342353047923185,-0.341816943064706,
-0.341278234841024,-0.340548126230012,-0.339006781639323,-0.336978302727952,
-0.332198752012145,-0.317035413522846,-0.303946243446485,-0.231170726504234,
-0.214521106857462,-0.185638263948231,-0.182579033906513,-0.181323329014338,
-0.180383230149897,-0.179350806895634,-0.177922239428873,-0.1745456798893,
-0.136176385911942,-0.037752960116968,-0.0342634325543829,-0.0338225101078654,
-0.0321021075804736,-0.0213809779737077,-0.0199861799137145,-0.019271842407949,
-0.0187447579747701,-0.0182119709174758,-0.0176494579022497,-0.0169022101124036,
-0.0157041435510641,-0.00096080709203007),.UNSPECIFIED.);
#143=B_SPLINE_CURVE_WITH_KNOTS('',3,(#24614,#24615,#24616,#24617,#24618,
#24619,#24620,#24621,#24622,#24623,#24624,#24625,#24626,#24627,#24628,#24629,
#24630,#24631,#24632,#24633,#24634,#24635,#24636,#24637,#24638,#24639,#24640,
#24641,#24642,#24643,#24644,#24645,#24646,#24647,#24648,#24649,#24650,#24651,
#24652,#24653,#24654,#24655,#24656,#24657,#24658,#24659,#24660,#24661,#24662,
#24663,#24664,#24665,#24666,#24667,#24668,#24669,#24670,#24671,#24672,#24673,
#24674,#24675,#24676,#24677,#24678,#24679,#24680,#24681,#24682,#24683,#24684,
#24685,#24686,#24687,#24688,#24689,#24690,#24691,#24692,#24693,#24694,#24695,
#24696,#24697,#24698,#24699,#24700,#24701,#24702,#24703,#24704,#24705),
 .UNSPECIFIED.,.F.,.F.,(4,2,2,2,2,2,2,2,2,2,2,2,2,2,2,2,2,2,2,2,2,2,2,2,
2,2,2,2,2,2,2,2,2,2,2,2,2,2,2,2,2,2,2,2,2,4),(-4.06134520834936,-3.96837948446271,
-3.9364107850448,-3.92187733576561,-3.91951624335496,-3.91828247988687,
-3.91727798879559,-3.91627270178459,-3.91444486983007,-3.90872447596486,
-3.79049585550717,-3.76979665848526,-3.76230356525439,-3.7594789094282,
-3.75810271474695,-3.75728164958469,-3.75654128918839,-3.75598402753498,
-3.75544818963429,-3.75469930248761,-3.75274412429328,-3.72382050698897,
-3.71026053601232,-3.68639899843738,-3.63442545529601,-3.61208571490417,
-3.59892025391591,-3.59661980038905,-3.59539866077819,-3.59439459939926,
-3.59338140594459,-3.59151530522612,-3.58549063863911,-3.4693180023132,
-3.44878262753612,-3.44002310160713,-3.43685535994991,-3.43535805703827,
-3.43448728028723,-3.43371128428702,-3.43314755786976,-3.43262086474612,
-3.43190732131699,-3.43051485449375,-3.4198407493259,-3.40024812751307),
 .UNSPECIFIED.);
#144=B_SPLINE_CURVE_WITH_KNOTS('',3,(#24706,#24707,#24708,#24709,#24710,
#24711,#24712,#24713,#24714,#24715,#24716,#24717,#24718,#24719,#24720,#24721,
#24722,#24723,#24724,#24725,#24726,#24727,#24728,#24729,#24730,#24731,#24732,
#24733,#24734,#24735,#24736,#24737,#24738,#24739,#24740,#24741,#24742,#24743,
#24744,#24745,#24746,#24747,#24748,#24749,#24750,#24751,#24752,#24753,#24754,
#24755,#24756,#24757,#24758,#24759,#24760,#24761,#24762,#24763,#24764,#24765,
#24766,#24767,#24768,#24769,#24770,#24771,#24772,#24773,#24774,#24775,#24776,
#24777,#24778,#24779,#24780,#24781,#24782,#24783,#24784,#24785,#24786,#24787,
#24788,#24789,#24790,#24791,#24792,#24793,#24794,#24795,#24796,#24797,#24798,
#24799,#24800,#24801,#24802,#24803,#24804,#24805,#24806,#24807,#24808,#24809,
#24810,#24811,#24812,#24813,#24814,#24815,#24816,#24817,#24818,#24819,#24820,
#24821,#24822,#24823,#24824,#24825,#24826,#24827,#24828,#24829,#24830,#24831,
#24832,#24833,#24834,#24835,#24836,#24837,#24838,#24839,#24840,#24841,#24842,
#24843,#24844,#24845,#24846,#24847,#24848,#24849,#24850,#24851,#24852,#24853,
#24854,#24855,#24856,#24857,#24858,#24859,#24860,#24861,#24862,#24863,#24864,
#24865,#24866,#24867,#24868,#24869,#24870,#24871,#24872,#24873,#24874,#24875,
#24876,#24877,#24878,#24879,#24880,#24881,#24882,#24883,#24884,#24885,#24886,
#24887,#24888,#24889,#24890,#24891,#24892,#24893,#24894,#24895,#24896,#24897,
#24898,#24899,#24900,#24901,#24902,#24903,#24904,#24905,#24906,#24907,#24908,
#24909,#24910,#24911,#24912,#24913,#24914,#24915,#24916,#24917,#24918,#24919,
#24920,#24921,#24922,#24923,#24924,#24925,#24926,#24927,#24928,#24929,#24930,
#24931,#24932,#24933,#24934,#24935,#24936,#24937,#24938,#24939,#24940,#24941,
#24942,#24943,#24944,#24945,#24946,#24947,#24948,#24949,#24950,#24951,#24952,
#24953,#24954,#24955,#24956,#24957,#24958,#24959,#24960,#24961,#24962,#24963),
 .UNSPECIFIED.,.F.,.F.,(4,2,2,2,2,2,2,2,2,2,2,2,2,2,2,2,2,2,2,2,2,2,2,2,
2,2,2,2,2,2,2,2,2,2,2,2,2,2,2,2,2,2,2,2,2,2,2,2,2,2,2,2,2,2,2,2,2,2,2,2,
2,2,2,2,2,2,2,2,2,2,2,2,2,2,2,2,2,2,2,2,2,2,2,2,2,2,2,2,2,2,2,2,2,2,2,2,
2,2,2,2,2,2,2,2,2,2,2,2,2,2,2,2,2,2,2,2,2,2,2,2,2,2,2,2,2,2,2,2,4),(-2.69413699669498,
-2.65797776204501,-2.56931048756278,-2.56543521196518,-2.5643842166337,
-2.56375429385175,-2.56324910870668,-2.56255451391301,-2.56149139705641,
-2.55680783167898,-2.46801353521712,-2.40813218440491,-2.40561640634868,
-2.4041207825857,-2.40277371487563,-2.40176817375987,-2.40081836411621,
-2.39952637163187,-2.39632998847909,-2.36084875337876,-2.33231101723818,
-2.31117440016871,-2.26557826022934,-2.25003376666667,-2.24260966383499,
-2.24132123523769,-2.24063926694692,-2.24008393596067,-2.23951281047455,
-2.23844129049829,-2.2348197614001,-2.17592014514316,-2.12654974716623,
-2.08424067310959,-2.08106316752288,-2.07966882575442,-2.07864183293595,
-2.07769311971313,-2.07640537097843,-2.07388564174684,-2.05412065468879,
-2.04780444377394,-2.03225337437467,-1.9834337411955,-1.93172019386119,
-1.91994713227829,-1.91851341140619,-1.91778884323659,-1.91725887431838,
-1.91668497125008,-1.91589575837881,-1.91405334140259,-1.86842143808323,
-1.76504935290494,-1.75883181450551,-1.75694085555721,-1.75592174891191,
-1.75492619560002,-1.75371468991757,-1.75146410969886,-1.73934326474796,
-1.71542218993718,-1.66983139631379,-1.59983232496637,-1.59583271754432,
-1.59473265491292,-1.59408541648728,-1.59353514947438,-1.59285742383072,
-1.59212330276364,-1.59095696848503,-1.58870581325269,-1.56718073530101,
-1.54317890354222,-1.50380677742589,-1.438992685355,-1.43503797408942,-1.43362346308503,
-1.43264085978811,-1.4317310357451,-1.4304943134161,-1.42812538488915,-1.41347923261291,
-1.38108711810398,-1.32996150914465,-1.2759824527835,-1.27258227925585,
-1.2715369193024,-1.27097109186211,-1.27042111694214,-1.26974708236269,
-1.26901862253513,-1.2678658018507,-1.26565047210073,-1.24470459842785,
-1.22298393026765,-1.11866745130031,-1.11241699140463,-1.11052222025656,
-1.10950239922201,-1.10850697640287,-1.10729680437512,-1.10505214411997,
-1.09304078830953,-1.06935809579366,-1.02396750534711,-0.964205306191557,
-0.950353234860537,-0.948852988011463,-0.948111730139071,-0.947577462289241,
-0.947018098770191,-0.946289924464967,-0.945467787321109,-0.944089852382067,
-0.941261804712596,-0.93376064929237,-0.902449198161415,-0.795457231966841,
-0.789166929538688,-0.787267626220621,-0.786133589670826,-0.785225835029717,
-0.784005988649509,-0.781715658909512,-0.7688016245874,-0.744143923004743,
-0.69298902551095,-0.66256616552324),.UNSPECIFIED.);
#145=B_SPLINE_CURVE_WITH_KNOTS('',3,(#24968,#24969,#24970,#24971,#24972,
#24973,#24974,#24975,#24976,#24977,#24978,#24979,#24980,#24981,#24982,#24983,
#24984,#24985,#24986,#24987,#24988,#24989,#24990,#24991,#24992,#24993,#24994,
#24995,#24996,#24997,#24998,#24999,#25000,#25001,#25002,#25003,#25004,#25005,
#25006,#25007,#25008,#25009,#25010,#25011,#25012,#25013,#25014,#25015,#25016,
#25017,#25018,#25019,#25020,#25021,#25022,#25023,#25024,#25025,#25026,#25027,
#25028,#25029,#25030,#25031,#25032,#25033,#25034,#25035,#25036,#25037,#25038,
#25039,#25040,#25041,#25042,#25043,#25044,#25045,#25046,#25047,#25048,#25049,
#25050,#25051,#25052,#25053,#25054,#25055,#25056,#25057,#25058,#25059,#25060,
#25061,#25062,#25063,#25064,#25065,#25066,#25067,#25068,#25069,#25070,#25071,
#25072,#25073,#25074,#25075,#25076,#25077,#25078,#25079,#25080,#25081,#25082,
#25083,#25084,#25085,#25086,#25087,#25088,#25089,#25090,#25091,#25092,#25093,
#25094,#25095,#25096,#25097,#25098,#25099,#25100,#25101,#25102,#25103,#25104,
#25105,#25106,#25107,#25108,#25109,#25110,#25111,#25112,#25113,#25114,#25115,
#25116,#25117,#25118,#25119,#25120,#25121,#25122,#25123,#25124,#25125,#25126,
#25127,#25128,#25129,#25130,#25131,#25132,#25133,#25134,#25135,#25136,#25137,
#25138,#25139,#25140,#25141,#25142,#25143,#25144,#25145,#25146,#25147,#25148,
#25149,#25150,#25151,#25152,#25153,#25154,#25155,#25156,#25157,#25158,#25159,
#25160,#25161,#25162,#25163,#25164,#25165,#25166,#25167,#25168,#25169,#25170,
#25171,#25172,#25173,#25174,#25175,#25176,#25177,#25178,#25179,#25180,#25181,
#25182,#25183,#25184,#25185,#25186,#25187,#25188,#25189,#25190,#25191,#25192,
#25193,#25194,#25195,#25196,#25197,#25198,#25199,#25200,#25201,#25202,#25203,
#25204,#25205,#25206,#25207,#25208,#25209,#25210,#25211,#25212,#25213,#25214,
#25215,#25216,#25217,#25218,#25219,#25220,#25221,#25222,#25223,#25224,#25225,
#25226,#25227,#25228,#25229,#25230,#25231,#25232,#25233,#25234,#25235),
 .UNSPECIFIED.,.F.,.F.,(4,2,2,2,2,2,2,2,2,2,2,2,2,2,2,2,2,2,2,2,2,2,2,2,
2,2,2,2,2,2,2,2,2,2,2,2,2,2,2,2,2,2,2,2,2,2,2,2,2,2,2,2,2,2,2,2,2,2,2,2,
2,2,2,2,2,2,2,2,2,2,2,2,2,2,2,2,2,2,2,2,2,2,2,2,2,2,2,2,2,2,2,2,2,2,2,2,
2,2,2,2,2,2,2,2,2,2,2,2,2,2,2,2,2,2,2,2,2,2,2,2,2,2,2,2,2,2,2,2,2,2,2,2,
2,4),(-3.40165445961574,-3.37651397343408,-3.31546800009253,-3.3055998640551,
-3.29396037018036,-3.26719634061028,-3.25311387375933,-3.25162047993218,
-3.25089653352018,-3.25038520291807,-3.24984664392857,-3.24908910657498,
-3.24752273708241,-3.23123774401991,-3.23022642079531,-3.22777500349404,
-3.13227826096747,-3.09785532997197,-3.09400584524469,-3.09197936447331,
-3.09068857816998,-3.08948930936203,-3.08850363838942,-3.08749657854455,
-3.08566417248586,-3.07991939968857,-2.96163122907052,-2.95278662553835,
-2.93700132916986,-2.92939720600353,-2.92810061813168,-2.92741701828514,
-2.92686174596242,-2.92620572969147,-2.92506768209998,-2.92068870539787,
-2.91803591657381,-2.91645773231244,-2.91509026791511,-2.82059313048553,
-2.77564341861965,-2.77114935357919,-2.7688796939199,-2.76748663922636,
-2.76621237580926,-2.7652188597922,-2.76424628694146,-2.76258668675173,
-2.7580812877869,-2.68495853290408,-2.63437171567505,-2.61050859690884,
-2.60585756064919,-2.60473925821006,-2.60409447560672,-2.60353297882944,
-2.60283249502999,-2.60174998251649,-2.5968239649577,-2.5011547536028,-2.45274112610681,
-2.44807013939555,-2.44573516061797,-2.44431484185283,-2.44302214861118,
-2.44202576751674,-2.44106056102874,-2.43970897634766,-2.43615578235766,
-2.43448157044393,-2.3576469212505,-2.33098899209477,-2.29861840213104,
-2.28331145355877,-2.28179484072996,-2.28106630172311,-2.28055423752006,
-2.28001724589956,-2.27926553826187,-2.27729565075319,-2.24748171454464,
-2.16024537730253,-2.13625534223526,-2.12319767711703,-2.1209005669633,
-2.11967934854468,-2.11877153337843,-2.11778189287501,-2.11603620855763,
-2.11094079922776,-2.03141703483579,-1.96353232804275,-1.95945518807607,
-1.95834730569696,-1.95769835664803,-1.95713730476804,-1.95644257414832,
-1.95509281509891,-1.94621081317906,-1.92494782026015,-1.87578506546496,
-1.82511041445525,-1.82150465774966,-1.80093991482197,-1.79810903878438,
-1.7967937601229,-1.7957762479802,-1.7946788091398,-1.79294316156894,-1.78740991264778,
-1.75568061070349,-1.70995083999306,-1.64042837910348,-1.6363908266861,
-1.63528697858705,-1.63463894565946,-1.63408883271241,-1.63341233050254,
-1.63267997428938,-1.63151771686193,-1.62927718663556,-1.60792121829486,
-1.58417470245642,-1.48202673335687,-1.47606685813653,-1.47420745542301,
-1.47319491108913,-1.47218959857971,-1.47096419336311,-1.46864747618132,
-1.45517478309306,-1.43885884009542,-1.41487041060513,-1.37029241472368),
 .UNSPECIFIED.);
#146=B_SPLINE_CURVE_WITH_KNOTS('',3,(#25237,#25238,#25239,#25240,#25241,
#25242,#25243,#25244,#25245,#25246,#25247,#25248,#25249,#25250,#25251,#25252,
#25253,#25254,#25255,#25256,#25257,#25258,#25259,#25260,#25261,#25262,#25263,
#25264,#25265,#25266,#25267,#25268,#25269,#25270,#25271,#25272,#25273,#25274,
#25275,#25276,#25277,#25278,#25279,#25280,#25281,#25282,#25283,#25284,#25285,
#25286,#25287,#25288,#25289,#25290,#25291,#25292,#25293,#25294,#25295,#25296,
#25297,#25298,#25299,#25300,#25301,#25302,#25303,#25304,#25305,#25306,#25307,
#25308,#25309,#25310,#25311,#25312,#25313,#25314,#25315,#25316,#25317,#25318,
#25319,#25320,#25321,#25322,#25323,#25324,#25325,#25326,#25327,#25328,#25329,
#25330),.UNSPECIFIED.,.F.,.F.,(4,2,2,2,2,2,2,2,2,2,2,2,2,2,2,2,2,2,2,2,
2,2,2,2,2,2,2,2,2,2,2,2,2,2,2,2,2,2,2,2,2,2,2,2,2,2,4),(-0.66256616552324,
-0.650642016057342,-0.627475925094102,-0.62561516282241,-0.624881560281531,
-0.624349371729995,-0.623788924323196,-0.623032695985302,-0.622189761079398,
-0.620761154543921,-0.61779040074806,-0.609768495821252,-0.589501938977944,
-0.471571106734159,-0.465783642166481,-0.463945924216361,-0.462937861064067,
-0.461932304695768,-0.460699741725335,-0.458348635350572,-0.444099907637023,
-0.413458500453692,-0.36897150926728,-0.347330245893649,-0.311466084634063,
-0.310602870351287,-0.303457661623643,-0.302227387371033,-0.301489951931337,
-0.300934018935329,-0.300333286097983,-0.299387675320691,-0.29646845572393,
-0.29192714869184,-0.277672888677262,-0.250982452063922,-0.148756806892039,
-0.142772884609283,-0.140910911626179,-0.139898067918963,-0.138893155076745,
-0.137669246928664,-0.135358390084581,-0.121999232846878,-0.119887552893688,
-0.0848123304289776,-0.000962485193680865),.UNSPECIFIED.);
#147=B_SPLINE_CURVE_WITH_KNOTS('',3,(#25331,#25332,#25333,#25334,#25335,
#25336,#25337,#25338,#25339,#25340,#25341,#25342,#25343,#25344,#25345,#25346,
#25347,#25348,#25349,#25350,#25351,#25352,#25353,#25354,#25355,#25356,#25357,
#25358,#25359,#25360,#25361,#25362,#25363,#25364,#25365,#25366,#25367,#25368,
#25369,#25370,#25371,#25372,#25373,#25374,#25375,#25376,#25377,#25378,#25379,
#25380,#25381,#25382,#25383,#25384,#25385,#25386,#25387,#25388,#25389,#25390,
#25391,#25392,#25393,#25394,#25395,#25396,#25397,#25398,#25399,#25400,#25401,
#25402,#25403,#25404,#25405,#25406,#25407,#25408,#25409,#25410,#25411,#25412,
#25413,#25414,#25415,#25416,#25417,#25418,#25419,#25420,#25421,#25422,#25423,
#25424,#25425,#25426,#25427,#25428,#25429,#25430,#25431,#25432,#25433,#25434,
#25435,#25436,#25437,#25438,#25439,#25440,#25441,#25442,#25443,#25444,#25445,
#25446,#25447,#25448,#25449,#25450,#25451,#25452,#25453,#25454,#25455,#25456,
#25457,#25458,#25459,#25460,#25461,#25462,#25463,#25464,#25465,#25466,#25467,
#25468,#25469,#25470,#25471,#25472,#25473,#25474,#25475,#25476,#25477,#25478,
#25479,#25480,#25481,#25482,#25483,#25484,#25485,#25486,#25487,#25488,#25489,
#25490,#25491,#25492,#25493,#25494,#25495,#25496,#25497,#25498,#25499,#25500,
#25501,#25502,#25503,#25504,#25505,#25506,#25507,#25508,#25509,#25510,#25511,
#25512,#25513,#25514,#25515,#25516,#25517,#25518,#25519,#25520,#25521,#25522,
#25523,#25524,#25525,#25526,#25527,#25528,#25529,#25530,#25531,#25532,#25533,
#25534,#25535,#25536,#25537,#25538,#25539,#25540,#25541,#25542,#25543,#25544,
#25545,#25546,#25547,#25548,#25549,#25550,#25551,#25552,#25553,#25554,#25555,
#25556),.UNSPECIFIED.,.F.,.F.,(4,2,2,2,2,2,2,2,2,2,2,2,2,2,2,2,2,2,2,2,
2,2,2,2,2,2,2,2,2,2,2,2,2,2,2,2,2,2,2,2,2,2,2,2,2,2,2,2,2,2,2,2,2,2,2,2,
2,2,2,2,2,2,2,2,2,2,2,2,2,2,2,2,2,2,2,2,2,2,2,2,2,2,2,2,2,2,2,2,2,2,2,2,
2,2,2,2,2,2,2,2,2,2,2,2,2,2,2,2,2,2,2,2,4),(-4.06163240503467,-4.04157573871171,
-4.04038201218937,-4.03963672300573,-4.0390750840685,-4.03854225091604,
-4.03801492403181,-4.03729886330514,-4.03589657414182,-4.02496218233544,
-4.02165983126325,-4.02093279376469,-4.01760821936916,-4.0140022612106,
-3.91647499154767,-3.89304517433229,-3.88114562152254,-3.87890888848764,
-3.87770131040074,-3.87679556589489,-3.87565467318111,-3.87372130724079,
-3.86712512399437,-3.8632839039215,-3.85934748122755,-3.85727724938406,
-3.85553286928691,-3.85431652569437,-3.85243683125332,-3.84515648624425,
-3.75504915554739,-3.73426065508786,-3.72343230095042,-3.71973263653401,
-3.71724397111261,-3.71635637203914,-3.71583160126477,-3.71526486181131,
-3.71452813641032,-3.71298339915092,-3.70187492498724,-3.69944465522738,
-3.65297477414986,-3.64811917839652,-3.64263042313296,-3.63634166400954,
-3.62901188123814,-3.59918788681215,-3.57227927282716,-3.5585504412355,
-3.55622343135512,-3.55499645190537,-3.5539918368805,-3.55298167272471,
-3.55113144962901,-3.5452382130096,-3.42856493187509,-3.40752233891435,
-3.39931294818784,-3.39629208498634,-3.39484607536417,-3.39367524510972,
-3.39302310729654,-3.39251844971999,-3.39195191389418,-3.39090135838375,
-3.38745295466888,-3.29862834838403,-3.28752756707905,-3.27293780923546,
-3.24825155902145,-3.23537512073953,-3.23308778798072,-3.23186909255781,
-3.23096200222637,-3.22982854702158,-3.22792962567114,-3.22163566559073,
-3.11531009309017,-3.09538121386358,-3.07959756646609,-3.07456765324311,
-3.07246130587609,-3.07135017461772,-3.07063941780253,-3.06997820865267,
-3.06942925963572,-3.06885594749971,-3.0677719646759,-3.06403533195082,
-3.06319326508204,-2.95986961545267,-2.91796811334442,-2.91140622988108,
-2.90955959352537,-2.90843781969178,-2.90742778519324,-2.90614173724338,
-2.90352964544845,-2.88103381242773,-2.86886802818526,-2.78493286844683,
-2.771758488508,-2.7516230394206,-2.74945952361181,-2.74832662820939,-2.74760674657255,
-2.74693941431449,-2.7463901610028,-2.74582137478078,-2.74475978602781,
-2.74121851702462,-2.69291085651066),.UNSPECIFIED.);
#148=B_SPLINE_CURVE_WITH_KNOTS('',3,(#25562,#25563,#25564,#25565,#25566,
#25567,#25568,#25569,#25570,#25571,#25572,#25573,#25574,#25575,#25576,#25577,
#25578,#25579,#25580,#25581,#25582,#25583,#25584,#25585,#25586,#25587,#25588,
#25589,#25590,#25591,#25592,#25593,#25594,#25595,#25596,#25597,#25598,#25599,
#25600,#25601,#25602,#25603,#25604,#25605,#25606,#25607,#25608,#25609,#25610,
#25611,#25612,#25613,#25614,#25615,#25616,#25617,#25618,#25619,#25620,#25621,
#25622,#25623,#25624,#25625,#25626,#25627,#25628,#25629,#25630,#25631,#25632,
#25633,#25634,#25635,#25636,#25637,#25638,#25639,#25640,#25641,#25642,#25643,
#25644,#25645,#25646,#25647,#25648,#25649,#25650,#25651,#25652,#25653,#25654,
#25655,#25656,#25657,#25658,#25659,#25660,#25661,#25662,#25663,#25664,#25665,
#25666,#25667,#25668,#25669,#25670,#25671,#25672,#25673,#25674,#25675,#25676,
#25677,#25678,#25679,#25680,#25681,#25682,#25683,#25684,#25685,#25686,#25687,
#25688,#25689,#25690,#25691,#25692,#25693,#25694,#25695,#25696,#25697,#25698,
#25699,#25700,#25701,#25702,#25703,#25704,#25705,#25706,#25707,#25708,#25709,
#25710,#25711,#25712,#25713,#25714,#25715,#25716,#25717,#25718,#25719,#25720,
#25721,#25722,#25723,#25724,#25725,#25726,#25727,#25728,#25729,#25730,#25731,
#25732,#25733,#25734,#25735,#25736,#25737,#25738,#25739,#25740,#25741,#25742,
#25743,#25744,#25745),.UNSPECIFIED.,.F.,.F.,(4,2,2,2,2,2,2,2,2,2,2,2,2,
2,2,2,2,2,2,2,2,2,2,2,2,2,2,2,2,2,2,2,2,2,2,2,2,2,2,2,2,2,2,2,2,2,2,2,2,
2,2,2,2,2,2,2,2,2,2,2,2,2,2,2,2,2,2,2,2,2,2,2,2,2,2,2,2,2,2,2,2,2,2,2,2,
2,2,2,2,2,2,4),(-1.36994082487413,-1.29603031198163,-1.29492405155685,-1.29097890040597,
-1.28956651607252,-1.28858499749473,-1.28759533239186,-1.2863455444552,
-1.28498602773553,-1.28279577186211,-1.23873322779561,-1.18847552089364,
-1.13212801695096,-1.12865639430014,-1.1276029913557,-1.12703583714301,
-1.12647537588788,-1.12578597295757,-1.12446063616401,-1.11618252681527,
-1.09815219310377,-1.06594107454888,-0.997095234521415,-0.984161026241984,
-0.983254624225425,-0.969794336805012,-0.967354308988684,-0.966076315947826,
-0.965087812338502,-0.963990292039223,-0.962843346257242,-0.961158379590627,
-0.946133958449461,-0.912221055408388,-0.834128051109883,-0.807182576143023,
-0.805256765335285,-0.804512362897235,-0.803977473044589,-0.80340764905284,
-0.802639959516383,-0.800915790566093,-0.754767053782881,-0.721703380028494,
-0.719073473633127,-0.688566799212006,-0.648197139496502,-0.644909582623209,
-0.643602521349625,-0.642649333299487,-0.64164720603178,-0.640314730180309,
-0.638840954602102,-0.636377016551929,-0.585924081096949,-0.504414296391204,
-0.501348766352125,-0.500210244449823,-0.483903780959305,-0.482337225289159,
-0.481579752799313,-0.48104130908245,-0.480530146495798,-0.479806531466997,
-0.478314176922611,-0.464265304664495,-0.437612850160603,-0.374178376701174,
-0.325373235946942,-0.321959878370101,-0.320631548344275,-0.319672724424056,
-0.318673671339005,-0.317360235912869,-0.315912921617537,-0.313512805330025,
-0.264500142443476,-0.17001048278854,-0.168371874730889,-0.16694049061098,
-0.164941408620806,-0.159977242239485,-0.158891862606302,-0.158190569316189,
-0.157629121469594,-0.156985167881734,-0.155870201828929,-0.151258814046137,
-0.112526851773713,-0.00998850380131196,-0.00354524911410741,-0.00096169998764838),
 .UNSPECIFIED.);
#149=B_SPLINE_CURVE_WITH_KNOTS('',3,(#25746,#25747,#25748,#25749,#25750,
#25751,#25752,#25753,#25754,#25755,#25756,#25757,#25758,#25759,#25760,#25761,
#25762,#25763,#25764,#25765,#25766,#25767,#25768,#25769,#25770,#25771,#25772,
#25773,#25774,#25775,#25776,#25777,#25778,#25779,#25780,#25781,#25782,#25783,
#25784,#25785,#25786,#25787,#25788,#25789,#25790,#25791,#25792,#25793,#25794,
#25795,#25796,#25797,#25798,#25799,#25800,#25801,#25802,#25803,#25804,#25805,
#25806,#25807,#25808,#25809,#25810,#25811,#25812,#25813,#25814,#25815,#25816,
#25817,#25818,#25819,#25820,#25821,#25822,#25823,#25824,#25825,#25826,#25827,
#25828,#25829,#25830,#25831,#25832,#25833,#25834,#25835,#25836,#25837,#25838,
#25839,#25840,#25841,#25842,#25843,#25844,#25845,#25846,#25847),
 .UNSPECIFIED.,.F.,.F.,(4,2,2,2,2,2,2,2,2,2,2,2,2,2,2,2,2,2,2,2,2,2,2,2,
2,2,2,2,2,2,2,2,2,2,2,2,2,2,2,2,2,2,2,2,2,2,2,2,2,2,4),(-4.06334679065876,
-4.0614676879816,-4.06023683188313,-4.0592641980323,-4.05827705711106,-4.05728978078462,
-4.05555580478751,-4.05054278406359,-4.02655588148113,-3.93101169180052,
-3.9028098550946,-3.89882546095418,-3.89776450235261,-3.89713252793102,
-3.89656917207661,-3.89584901909655,-3.89470271198501,-3.88891192429347,
-3.88757741407342,-3.88650615930939,-3.88473245356577,-3.79028214035835,
-3.74549045229745,-3.74100514892433,-3.73873880066728,-3.73734717590536,
-3.73607402101243,-3.73508072801975,-3.73410790828129,-3.73272815964916,
-3.72899836538777,-3.66801956698602,-3.57943188427975,-3.5755380354782,
-3.57448554566139,-3.5738554466752,-3.57329168545548,-3.57256820155787,
-3.57107737979007,-3.56680112404204,-3.46927446488557,-3.42239407658512,
-3.417798908159,-3.41549186252672,-3.41408320032954,-3.41279768493003,-3.41180262857148,
-3.41083425782256,-3.40947097156366,-3.40664913081027,-3.40165445961574),
 .UNSPECIFIED.);
#150=B_SPLINE_CURVE_WITH_KNOTS('',3,(#25848,#25849,#25850,#25851,#25852,
#25853,#25854,#25855,#25856,#25857,#25858,#25859,#25860,#25861,#25862,#25863,
#25864,#25865,#25866,#25867,#25868,#25869,#25870,#25871,#25872,#25873,#25874,
#25875,#25876,#25877,#25878,#25879,#25880,#25881,#25882,#25883,#25884,#25885,
#25886,#25887,#25888,#25889,#25890,#25891,#25892,#25893,#25894,#25895,#25896,
#25897,#25898,#25899,#25900,#25901,#25902,#25903,#25904,#25905,#25906,#25907,
#25908,#25909,#25910,#25911,#25912,#25913,#25914,#25915,#25916,#25917,#25918,
#25919,#25920,#25921,#25922,#25923,#25924,#25925,#25926,#25927,#25928,#25929,
#25930,#25931,#25932,#25933,#25934,#25935,#25936,#25937,#25938,#25939,#25940,
#25941,#25942,#25943,#25944,#25945,#25946,#25947,#25948,#25949,#25950,#25951,
#25952,#25953,#25954,#25955,#25956,#25957,#25958,#25959,#25960,#25961,#25962,
#25963,#25964,#25965,#25966,#25967,#25968,#25969,#25970,#25971,#25972,#25973,
#25974,#25975,#25976,#25977,#25978,#25979,#25980,#25981,#25982,#25983,#25984,
#25985,#25986,#25987,#25988,#25989,#25990,#25991,#25992,#25993,#25994,#25995,
#25996,#25997,#25998,#25999,#26000,#26001,#26002,#26003,#26004,#26005,#26006,
#26007,#26008,#26009,#26010,#26011,#26012,#26013,#26014,#26015,#26016,#26017,
#26018,#26019,#26020,#26021,#26022,#26023,#26024,#26025,#26026,#26027,#26028,
#26029,#26030,#26031,#26032,#26033,#26034,#26035,#26036,#26037,#26038,#26039,
#26040,#26041,#26042,#26043,#26044,#26045,#26046,#26047,#26048,#26049,#26050,
#26051,#26052,#26053,#26054,#26055,#26056,#26057,#26058,#26059,#26060,#26061,
#26062,#26063,#26064,#26065,#26066,#26067,#26068,#26069,#26070,#26071,#26072,
#26073,#26074,#26075,#26076,#26077,#26078,#26079,#26080,#26081,#26082,#26083,
#26084,#26085,#26086,#26087,#26088,#26089,#26090,#26091,#26092,#26093,#26094,
#26095,#26096,#26097,#26098,#26099,#26100,#26101,#26102,#26103,#26104,#26105,
#26106,#26107),.UNSPECIFIED.,.F.,.F.,(4,2,2,2,2,2,2,2,2,2,2,2,2,2,2,2,2,
2,2,2,2,2,2,2,2,2,2,2,2,2,2,2,2,2,2,2,2,2,2,2,2,2,2,2,2,2,2,2,2,2,2,2,2,
2,2,2,2,2,2,2,2,2,2,2,2,2,2,2,2,2,2,2,2,2,2,2,2,2,2,2,2,2,2,2,2,2,2,2,2,
2,2,2,2,2,2,2,2,2,2,2,2,2,2,2,2,2,2,2,2,2,2,2,2,2,2,2,2,2,2,2,2,2,2,2,2,
2,2,2,2,4),(-2.69291085651066,-2.68483550196456,-2.63175781315807,-2.59453214581927,
-2.58842111889877,-2.58662122692198,-2.58550985634893,-2.58449730481997,
-2.58319143929397,-2.58048011880597,-2.5627341192017,-2.56070138624403,
-2.5554977272015,-2.47750698729298,-2.42871120830902,-2.4265515182855,-2.42542005379274,
-2.42470075482836,-2.42403387557628,-2.42347995758067,-2.42290948848786,
-2.42183967505021,-2.41822796826577,-2.3584291822467,-2.33287252748695,
-2.30398635587902,-2.27929043290245,-2.26641354891322,-2.26412582489114,
-2.26290688320973,-2.26190225157808,-2.26088645654468,-2.25900968153982,
-2.25290365961186,-2.14298108650705,-2.1045499646331,-2.10215219233093,
-2.10127492902509,-2.10068374611877,-2.10011010983474,-2.09941837242733,
-2.09769057906015,-2.08181125684333,-2.08043691419415,-2.07839069856121,
-2.03210973013485,-1.94744299533067,-1.94224607278765,-1.9404864877677,
-1.93949420115805,-1.93858713024149,-1.93737161160444,-1.93510041509311,
-1.92256147488824,-1.89789957648225,-1.80996532116847,-1.8062218569041,
-1.79586973230887,-1.79507323407456,-1.79354893993996,-1.79281544358036,
-1.79154642977009,-1.78029833685377,-1.77872725313645,-1.77799612124083,
-1.77742988718088,-1.77681056963108,-1.77580567093845,-1.77238181189004,
-1.75059182328577,-1.72632260840022,-1.67037088712027,-1.62202120263258,
-1.61861268862138,-1.61716706029754,-1.61614241426979,-1.61519354646335,
-1.61417263921128,-1.61161591158002,-1.59135857889265,-1.5588587626773,
-1.46137199625791,-1.45696788098358,-1.45557285966385,-1.45485925454564,
-1.45429662086237,-1.45366071900825,-1.45258211618047,-1.44840291232943,
-1.41756323602812,-1.30205182218662,-1.29607304721407,-1.2942487356737,
-1.29313690631429,-1.29214303502324,-1.29117456508021,-1.28913758390785,
-1.28039658225398,-1.26477103761199,-1.24223401994546,-1.19147447850136,
-1.1362534129299,-1.1330601389816,-1.13204086129924,-1.1314804921133,-1.13092437392153,
-1.13022495392216,-1.12885214501725,-1.11932666108276,-1.09083100733912,
-1.00240288889988,-0.975035052016722,-0.972038341799565,-0.970670524523666,
-0.969661761801333,-0.96871831060029,-0.967675708467565,-0.964911838216675,
-0.93420291292175,-0.922831668509246,-0.838592420836438,-0.81150048814873,
-0.809572003159847,-0.808827057408071,-0.808291942922505,-0.807722040540725,
-0.806954514568413,-0.805231830163798,-0.759955563739871,-0.662267969628587),
 .UNSPECIFIED.);
#151=B_SPLINE_CURVE_WITH_KNOTS('',3,(#26112,#26113,#26114,#26115,#26116,
#26117,#26118,#26119,#26120,#26121,#26122,#26123,#26124,#26125,#26126,#26127,
#26128,#26129,#26130,#26131,#26132,#26133,#26134,#26135,#26136,#26137,#26138,
#26139,#26140,#26141,#26142,#26143,#26144,#26145,#26146,#26147,#26148,#26149,
#26150,#26151,#26152,#26153,#26154,#26155,#26156,#26157,#26158,#26159,#26160,
#26161,#26162,#26163,#26164,#26165,#26166,#26167,#26168,#26169,#26170,#26171,
#26172,#26173,#26174,#26175,#26176,#26177,#26178,#26179,#26180,#26181,#26182,
#26183,#26184,#26185,#26186,#26187,#26188,#26189,#26190,#26191,#26192,#26193,
#26194,#26195,#26196,#26197,#26198,#26199,#26200,#26201,#26202,#26203,#26204,
#26205,#26206,#26207,#26208,#26209,#26210,#26211,#26212,#26213,#26214,#26215,
#26216,#26217,#26218,#26219,#26220,#26221,#26222,#26223,#26224,#26225,#26226,
#26227,#26228,#26229,#26230,#26231,#26232,#26233,#26234,#26235,#26236,#26237,
#26238,#26239,#26240,#26241,#26242,#26243,#26244,#26245,#26246,#26247,#26248,
#26249,#26250,#26251,#26252,#26253,#26254,#26255,#26256,#26257,#26258,#26259,
#26260,#26261,#26262,#26263,#26264,#26265,#26266,#26267,#26268,#26269,#26270,
#26271,#26272,#26273,#26274,#26275,#26276,#26277,#26278,#26279,#26280,#26281,
#26282,#26283,#26284,#26285,#26286,#26287,#26288,#26289,#26290,#26291,#26292,
#26293,#26294,#26295,#26296,#26297,#26298,#26299,#26300,#26301,#26302,#26303,
#26304,#26305,#26306,#26307,#26308,#26309,#26310,#26311,#26312,#26313,#26314,
#26315,#26316,#26317,#26318,#26319,#26320,#26321,#26322,#26323,#26324,#26325,
#26326,#26327,#26328,#26329,#26330,#26331,#26332,#26333,#26334,#26335,#26336,
#26337,#26338,#26339,#26340,#26341,#26342,#26343,#26344,#26345,#26346,#26347,
#26348,#26349,#26350,#26351,#26352,#26353,#26354,#26355,#26356,#26357,#26358,
#26359,#26360,#26361,#26362,#26363,#26364,#26365,#26366,#26367,#26368,#26369,
#26370,#26371,#26372,#26373,#26374,#26375,#26376,#26377,#26378,#26379,#26380,
#26381,#26382,#26383,#26384,#26385,#26386,#26387,#26388,#26389,#26390,#26391,
#26392,#26393,#26394,#26395,#26396,#26397,#26398,#26399,#26400,#26401,#26402,
#26403,#26404,#26405,#26406,#26407,#26408,#26409,#26410,#26411),
 .UNSPECIFIED.,.F.,.F.,(4,2,2,2,2,2,2,2,2,2,2,2,2,2,2,2,2,2,2,2,2,2,2,2,
2,2,2,2,2,2,2,2,2,2,2,2,2,2,2,2,2,2,2,2,2,2,2,2,2,2,2,2,2,2,2,2,2,2,2,2,
2,2,2,2,2,2,2,2,2,2,2,2,2,2,2,2,2,2,2,2,2,2,2,2,2,2,2,2,2,2,2,2,2,2,2,2,
2,2,2,2,2,2,2,2,2,2,2,2,2,2,2,2,2,2,2,2,2,2,2,2,2,2,2,2,2,2,2,2,2,2,2,2,
2,2,2,2,2,2,2,2,2,2,2,2,2,2,2,2,2,4),(-3.39905562805101,-3.3986699384756,
-3.39720180526091,-3.39190640431446,-3.38971888762928,-3.38808097034261,
-3.38733247960283,-3.3867986607061,-3.38626974911432,-3.38554728983858,
-3.38411974379569,-3.37248028154884,-3.28933011170741,-3.27783349011705,
-3.24888080575984,-3.22995922470087,-3.22744230425333,-3.2261759310716,
-3.22526332232139,-3.22429554298103,-3.22293194666987,-3.22010574508331,
-3.18963746712672,-3.10268644497334,-3.07632509123859,-3.06978633775776,
-3.06723084153549,-3.06595196616715,-3.06517117168965,-3.06445971556827,
-3.06390666882451,-3.06336054141764,-3.06241065271926,-3.05972482703521,
-3.01720005158188,-2.98411126843357,-2.94025091241868,-2.91100757322446,
-2.90575142860157,-2.90405015562316,-2.90296108636246,-2.90194193229755,
-2.90061112298654,-2.8978003724413,-2.87676775237228,-2.87420551087048,
-2.8583565003042,-2.79843755596687,-2.74624998893677,-2.74414329951607,
-2.74303218260706,-2.74232154754129,-2.74169176920089,-2.74114234503394,
-2.74057827571828,-2.73953932909358,-2.73618511443869,-2.68283241446274,
-2.62323973103681,-2.5889514290326,-2.58314482637424,-2.58137887768191,
-2.58027540224033,-2.57926122580341,-2.57796263625027,-2.5752148524396,
-2.55662202539812,-2.55510995371541,-2.54833664258733,-2.4715202614367,
-2.46071833832439,-2.42215998939823,-2.42070194060178,-2.41984719434025,
-2.41908319135597,-2.41852160291228,-2.4179923249728,-2.41726865202679,
-2.4158365566108,-2.40407091510391,-2.37530191281133,-2.35692500368991,
-2.32727054756971,-2.29077996059181,-2.27139508429334,-2.26112417283738,
-2.25898218897382,-2.25779504572126,-2.25689071284536,-2.25588258531324,
-2.25404245997039,-2.24823003307144,-2.13068933116611,-2.10156316604489,
-2.09889049714317,-2.09695468628881,-2.09614988910252,-2.09557355722074,
-2.09504774530097,-2.0943380789986,-2.09296103325885,-2.08268953884468,
-2.08086863707242,-2.07784366970475,-2.07654119765468,-2.03125364127204,
-1.99906316433315,-1.97884394746461,-1.97161463890321,-1.93973307258011,
-1.93662013100313,-1.93534346946044,-1.93439818211379,-1.9333703030968,
-1.93196653990711,-1.92873164333418,-1.88020924667334,-1.7879215533845,
-1.78657229472881,-1.77542135151552,-1.77387436359239,-1.77313696918752,
-1.77256989857996,-1.77195380463532,-1.77096289000188,-1.76766602530795,
-1.74718532434993,-1.73396230204563,-1.64632871888124,-1.61659057824934,
-1.61353052414316,-1.61226317438258,-1.61132017450241,-1.61032300956624,
-1.60895754589759,-1.60743792718969,-1.60486296867588,-1.56146999677902,
-1.51111495076938,-1.45500715430153,-1.45157858195507,-1.45053031726415,
-1.44996419452574,-1.44940362642723,-1.44871245411735,-1.44737871334427,
-1.43889460717303,-1.41946963007192,-1.37324998273249,-1.36994082487413),
 .UNSPECIFIED.);
#152=B_SPLINE_CURVE_WITH_KNOTS('',3,(#26413,#26414,#26415,#26416,#26417,
#26418,#26419,#26420,#26421,#26422,#26423,#26424,#26425,#26426,#26427,#26428,
#26429,#26430,#26431,#26432,#26433,#26434,#26435,#26436,#26437,#26438,#26439,
#26440,#26441,#26442,#26443,#26444,#26445,#26446,#26447,#26448,#26449,#26450,
#26451,#26452,#26453,#26454,#26455,#26456,#26457,#26458,#26459,#26460,#26461,
#26462,#26463,#26464,#26465,#26466,#26467,#26468,#26469,#26470,#26471,#26472,
#26473,#26474,#26475,#26476,#26477,#26478,#26479,#26480,#26481,#26482,#26483,
#26484,#26485,#26486,#26487,#26488,#26489,#26490,#26491,#26492,#26493,#26494,
#26495,#26496,#26497,#26498,#26499,#26500,#26501,#26502,#26503,#26504,#26505,
#26506,#26507,#26508,#26509,#26510,#26511,#26512),.UNSPECIFIED.,.F.,.F.,
(4,2,2,2,2,2,2,2,2,2,2,2,2,2,2,2,2,2,2,2,2,2,2,2,2,2,2,2,2,2,2,2,2,2,2,
2,2,2,2,2,2,2,2,2,2,2,2,2,2,4),(-0.662267969628587,-0.656023241631284,-0.649906582883767,
-0.64806596154954,-0.646950363692581,-0.645954340698451,-0.644987197316384,
-0.642963829703752,-0.634398844025601,-0.542932602219484,-0.497333269948792,
-0.495144278173578,-0.494245840517306,-0.490575941454874,-0.486880676462917,
-0.485801182679687,-0.485228684430029,-0.484724483902254,-0.484066939921601,
-0.482890258037996,-0.477437933404764,-0.467069832420578,-0.436585264058004,
-0.414257558544152,-0.389882563565053,-0.329821797885483,-0.326147117059869,
-0.324654368488396,-0.323619287580412,-0.322666199478999,-0.321655778378131,
-0.319198646559563,-0.302198934422417,-0.260708699561111,-0.175336862317592,
-0.16466336406662,-0.163270153193844,-0.162556139838001,-0.16202905573395,
-0.161453333567352,-0.160652932858231,-0.158744386743169,-0.156119409559968,
-0.127971580737986,-0.0317350575781189,-0.0223250194030482,-0.00512195002278438,
-0.00248768498826383,-0.00122476864328915,-0.000961573598619955),
 .UNSPECIFIED.);
#153=B_SPLINE_CURVE_WITH_KNOTS('',3,(#26513,#26514,#26515,#26516,#26517,
#26518,#26519,#26520,#26521,#26522,#26523,#26524,#26525,#26526,#26527,#26528,
#26529,#26530,#26531,#26532,#26533,#26534,#26535,#26536,#26537,#26538,#26539,
#26540,#26541,#26542,#26543,#26544,#26545,#26546,#26547,#26548,#26549,#26550,
#26551,#26552,#26553,#26554,#26555,#26556,#26557,#26558,#26559,#26560,#26561,
#26562,#26563,#26564,#26565,#26566,#26567,#26568,#26569,#26570,#26571,#26572,
#26573,#26574,#26575,#26576,#26577,#26578,#26579,#26580,#26581,#26582,#26583,
#26584,#26585,#26586,#26587,#26588,#26589,#26590,#26591,#26592,#26593,#26594,
#26595,#26596,#26597,#26598,#26599,#26600,#26601,#26602,#26603,#26604,#26605,
#26606,#26607,#26608,#26609,#26610,#26611,#26612,#26613,#26614,#26615,#26616,
#26617,#26618,#26619,#26620,#26621,#26622,#26623,#26624,#26625,#26626,#26627,
#26628,#26629,#26630,#26631,#26632,#26633,#26634,#26635,#26636,#26637,#26638,
#26639,#26640,#26641,#26642,#26643,#26644,#26645,#26646,#26647,#26648,#26649,
#26650,#26651,#26652,#26653,#26654,#26655,#26656,#26657,#26658,#26659,#26660,
#26661,#26662,#26663,#26664,#26665,#26666,#26667,#26668,#26669,#26670,#26671,
#26672,#26673,#26674,#26675,#26676,#26677,#26678,#26679,#26680,#26681,#26682,
#26683,#26684,#26685,#26686,#26687,#26688,#26689,#26690,#26691,#26692,#26693,
#26694,#26695,#26696),.UNSPECIFIED.,.F.,.F.,(4,2,2,2,2,2,2,2,2,2,2,2,2,
2,2,2,2,2,2,2,2,2,2,2,2,2,2,2,2,2,2,2,2,2,2,2,2,2,2,2,2,2,2,2,2,2,2,2,2,
2,2,2,2,2,2,2,2,2,2,2,2,2,2,2,2,2,2,2,2,2,2,2,2,2,2,2,2,2,2,2,2,2,2,2,2,
2,2,2,2,2,2,4),(-4.06231940115315,-4.06180759515383,-4.06079267865506,-4.05939540104,
-4.05624487799662,-4.0532022843239,-3.9424777929911,-3.90396032272885,-3.90156122198485,
-3.90068376038417,-3.90009253062331,-3.89951891829682,-3.89882728977886,
-3.89710018829005,-3.88124564745109,-3.83630906365861,-3.78677498115249,
-3.76088784226537,-3.74304340076237,-3.74055807558855,-3.73954468988837,
-3.73853530026321,-3.73759188141429,-3.73613538678742,-3.73266658508861,
-3.67873597587883,-3.64085397514781,-3.63143354367246,-3.60038961646899,
-3.58754743551197,-3.57947671512071,-3.5781598278382,-3.57747209254732,
-3.57691157692918,-3.57634315327523,-3.57528392699597,-3.57176455340614,
-3.51497871156925,-3.46492125578514,-3.4207589708795,-3.4178533296904,-3.41679587937533,
-3.41575921816129,-3.41474546475796,-3.41335356104129,-3.41023291768028,
-3.37806717194243,-3.32556928343734,-3.31603859829061,-3.30572739075148,
-3.29307842166342,-3.27327501218121,-3.26458607681714,-3.25654649446471,
-3.255230961657,-3.25454352106071,-3.25398303182519,-3.25332865876994,-3.25219700649735,
-3.24788046080548,-3.17371029214313,-3.13003583735646,-3.10097359772646,
-3.09573641244768,-3.09447138566884,-3.09329064532566,-3.09233920123119,
-3.09132991006396,-3.08955980118985,-3.0840167303125,-2.9646942651452,-2.95556621861452,
-2.94045892842583,-2.93323472331399,-2.93195626433792,-2.93127657644906,
-2.9307215382597,-2.93014932162394,-2.9290717029883,-2.92539458002595,-2.92412346345475,
-2.82631763989466,-2.80257022693576,-2.77707481939084,-2.77224766956423,
-2.77101389900872,-2.77004036023397,-2.76905108190309,-2.76806482889069,
-2.7664019721073,-2.76164844464432,-2.69296972658525),.UNSPECIFIED.);
#154=B_SPLINE_CURVE_WITH_KNOTS('',3,(#26702,#26703,#26704,#26705,#26706,
#26707,#26708,#26709,#26710,#26711,#26712,#26713,#26714,#26715,#26716,#26717,
#26718,#26719,#26720,#26721,#26722,#26723,#26724,#26725,#26726,#26727,#26728,
#26729,#26730,#26731,#26732,#26733,#26734,#26735,#26736,#26737,#26738,#26739,
#26740,#26741,#26742,#26743,#26744,#26745,#26746,#26747,#26748,#26749,#26750,
#26751,#26752,#26753,#26754,#26755,#26756,#26757,#26758,#26759,#26760,#26761,
#26762,#26763,#26764,#26765,#26766,#26767,#26768,#26769,#26770,#26771,#26772,
#26773,#26774,#26775,#26776,#26777,#26778,#26779,#26780,#26781,#26782,#26783,
#26784,#26785,#26786,#26787,#26788,#26789,#26790,#26791,#26792,#26793,#26794,
#26795,#26796,#26797,#26798,#26799,#26800,#26801,#26802,#26803,#26804,#26805,
#26806,#26807,#26808,#26809,#26810,#26811,#26812,#26813,#26814,#26815,#26816,
#26817,#26818,#26819,#26820,#26821,#26822,#26823,#26824,#26825,#26826,#26827,
#26828,#26829,#26830,#26831,#26832,#26833,#26834,#26835,#26836,#26837,#26838,
#26839,#26840,#26841,#26842,#26843,#26844,#26845,#26846,#26847,#26848,#26849,
#26850,#26851,#26852,#26853,#26854,#26855,#26856,#26857,#26858,#26859,#26860,
#26861,#26862,#26863,#26864,#26865,#26866,#26867,#26868,#26869,#26870,#26871,
#26872,#26873,#26874,#26875,#26876,#26877,#26878,#26879,#26880,#26881,#26882,
#26883,#26884,#26885,#26886,#26887,#26888,#26889,#26890,#26891,#26892,#26893,
#26894,#26895,#26896,#26897,#26898,#26899,#26900,#26901,#26902,#26903,#26904,
#26905,#26906,#26907),.UNSPECIFIED.,.F.,.F.,(4,2,2,2,2,2,2,2,2,2,2,2,2,
2,2,2,2,2,2,2,2,2,2,2,2,2,2,2,2,2,2,2,2,2,2,2,2,2,2,2,2,2,2,2,2,2,2,2,2,
2,2,2,2,2,2,2,2,2,2,2,2,2,2,2,2,2,2,2,2,2,2,2,2,2,2,2,2,2,2,2,2,2,2,2,2,
2,2,2,2,2,2,2,2,2,2,2,2,2,2,2,2,2,4),(-1.37023206616483,-1.36812966361624,
-1.31495988064365,-1.28033116872487,-1.26872960285219,-1.26730259113486,
-1.26657998762061,-1.26605077026252,-1.26548848956129,-1.26472150735698,
-1.26386347679314,-1.26239780624463,-1.21544819021846,-1.1932339046631,
-1.11272357861048,-1.10757180926247,-1.10581847031458,-1.10482746207289,
-1.10392019817567,-1.10270240312946,-1.10042043505791,-1.0876645510105,
-1.06285764487118,-0.973142332264336,-0.954735945592908,-0.953459607769599,
-0.951956994763824,-0.949186331896358,-0.944914352439075,-0.943787044256786,
-0.943133664459087,-0.942584157805125,-0.941914368128,-0.940664557757263,
-0.939097805969844,-0.93572985566497,-0.92620885310859,-0.899459465785207,
-0.790737433724329,-0.784595174758264,-0.782713971899396,-0.781697251055323,
-0.780692624614882,-0.779475013023821,-0.777193699614575,-0.76444906438141,
-0.739643230788104,-0.689662903122298,-0.625647408021433,-0.621708484638798,
-0.620615248209474,-0.61996986684673,-0.619412573859502,-0.618729544632254,
-0.617416517373076,-0.615752896765813,-0.612099286665519,-0.601457722911825,
-0.568140987320813,-0.498018646632726,-0.485493248689937,-0.482050548550778,
-0.47887318870941,-0.462939220777084,-0.460313579950492,-0.459024613167074,
-0.458014013093852,-0.456893387024039,-0.455052701898673,-0.44855281448265,
-0.407322099037772,-0.365246197278059,-0.344693621299669,-0.313483607794391,
-0.29972154074754,-0.29822460434893,-0.297484392501702,-0.296950603967475,
-0.296413443383186,-0.295677169972216,-0.294102935764683,-0.292021725646933,
-0.287073339626908,-0.271407256029271,-0.256206865639362,-0.166479195264413,
-0.16011771861926,-0.158437408867385,-0.157235944336469,-0.155485998957491,
-0.153424555031228,-0.149574665412683,-0.145998697765913,-0.144549876647307,
-0.138643839787367,-0.136791574428554,-0.135780742574086,-0.134775747228059,
-0.13354871754341,-0.13122286451297,-0.117534835788489,-0.0912986355765214,
-0.00096255119342937),.UNSPECIFIED.);
#155=B_SPLINE_CURVE_WITH_KNOTS('',3,(#26908,#26909,#26910,#26911,#26912,
#26913,#26914,#26915,#26916,#26917,#26918,#26919,#26920,#26921,#26922,#26923,
#26924,#26925,#26926,#26927,#26928,#26929,#26930,#26931,#26932,#26933,#26934,
#26935,#26936,#26937,#26938,#26939,#26940,#26941,#26942,#26943,#26944,#26945,
#26946,#26947,#26948,#26949,#26950,#26951,#26952,#26953,#26954,#26955,#26956,
#26957,#26958,#26959,#26960,#26961,#26962,#26963,#26964,#26965,#26966,#26967,
#26968,#26969,#26970,#26971,#26972,#26973,#26974,#26975,#26976,#26977,#26978,
#26979,#26980,#26981,#26982,#26983,#26984,#26985,#26986,#26987,#26988,#26989,
#26990,#26991,#26992,#26993,#26994,#26995,#26996,#26997,#26998,#26999,#27000,
#27001,#27002,#27003,#27004,#27005,#27006,#27007,#27008,#27009,#27010,#27011,
#27012,#27013,#27014,#27015,#27016,#27017,#27018,#27019,#27020,#27021,#27022,
#27023,#27024,#27025,#27026,#27027,#27028,#27029),.UNSPECIFIED.,.F.,.F.,
(4,2,2,2,2,2,2,2,2,2,2,2,2,2,2,2,2,2,2,2,2,2,2,2,2,2,2,2,2,2,2,2,2,2,2,
2,2,2,2,2,2,2,2,2,2,2,2,2,2,2,2,2,2,2,2,2,2,2,2,2,4),(-4.0595736983573,
-4.0360030272802,-4.03453647378078,-4.03367831943194,-4.03307303464023,
-4.03254841386927,-4.03198175256297,-4.03124476428623,-4.02964042551851,
-4.01750352546539,-4.01634326598266,-4.01342588961253,-4.01274888999768,
-4.01050484083728,-4.00742193864187,-4.00370322584028,-3.91043602532289,
-3.8869449413952,-3.8750189499694,-3.87278119696411,-3.87157357934867,-3.87057964726954,
-3.86956081603211,-3.86766630772408,-3.8614037040846,-3.75438676477088,
-3.73730444856761,-3.72003811725165,-3.71461238701461,-3.71238529077751,
-3.71072461678017,-3.70997120270708,-3.70943840622781,-3.70891107597547,
-3.70819473527818,-3.70679108071026,-3.69581484089607,-3.69255725567441,
-3.69215376896637,-3.68993429776076,-3.68876801112298,-3.68762958165876,
-3.64096361949087,-3.63570444608284,-3.62967232937953,-3.62264150764535,
-3.61425214983486,-3.58571416026584,-3.55647372490919,-3.55121806510108,
-3.54951693657518,-3.54842795659784,-3.54740888383224,-3.54607817745163,
-3.54326763255019,-3.52223617698608,-3.51967663428222,-3.50304470260634,
-3.4439490838304,-3.41116981593671,-3.39905562805101),.UNSPECIFIED.);
#156=B_SPLINE_CURVE_WITH_KNOTS('',3,(#27030,#27031,#27032,#27033,#27034,
#27035,#27036,#27037,#27038,#27039,#27040,#27041,#27042,#27043,#27044,#27045,
#27046,#27047,#27048,#27049,#27050,#27051,#27052,#27053,#27054,#27055,#27056,
#27057,#27058,#27059,#27060,#27061,#27062,#27063,#27064,#27065,#27066,#27067,
#27068,#27069,#27070,#27071,#27072,#27073,#27074,#27075,#27076,#27077,#27078,
#27079,#27080,#27081,#27082,#27083,#27084,#27085,#27086,#27087,#27088,#27089,
#27090,#27091,#27092,#27093,#27094,#27095,#27096,#27097,#27098,#27099,#27100,
#27101,#27102,#27103,#27104,#27105,#27106,#27107,#27108,#27109,#27110,#27111,
#27112,#27113,#27114,#27115,#27116,#27117,#27118,#27119,#27120,#27121,#27122,
#27123,#27124,#27125,#27126,#27127,#27128,#27129,#27130,#27131,#27132,#27133,
#27134,#27135,#27136,#27137,#27138,#27139,#27140,#27141,#27142,#27143,#27144,
#27145,#27146,#27147,#27148,#27149,#27150,#27151,#27152,#27153,#27154,#27155,
#27156,#27157,#27158,#27159,#27160,#27161,#27162,#27163,#27164,#27165,#27166,
#27167,#27168,#27169,#27170,#27171,#27172,#27173,#27174,#27175,#27176,#27177,
#27178,#27179,#27180,#27181,#27182,#27183,#27184,#27185,#27186,#27187,#27188,
#27189,#27190,#27191,#27192,#27193,#27194,#27195,#27196,#27197,#27198,#27199,
#27200,#27201,#27202,#27203,#27204,#27205,#27206,#27207,#27208,#27209,#27210,
#27211,#27212,#27213,#27214,#27215,#27216,#27217,#27218,#27219,#27220,#27221,
#27222,#27223,#27224,#27225,#27226,#27227,#27228,#27229,#27230,#27231,#27232,
#27233,#27234,#27235,#27236,#27237,#27238,#27239,#27240,#27241,#27242,#27243,
#27244,#27245,#27246,#27247,#27248,#27249,#27250,#27251,#27252,#27253,#27254,
#27255,#27256,#27257,#27258,#27259,#27260,#27261,#27262,#27263,#27264,#27265,
#27266,#27267,#27268,#27269,#27270,#27271,#27272,#27273,#27274,#27275,#27276,
#27277,#27278,#27279,#27280,#27281,#27282,#27283,#27284,#27285,#27286,#27287,
#27288,#27289,#27290,#27291,#27292,#27293,#27294,#27295,#27296,#27297,#27298,
#27299,#27300,#27301,#27302,#27303,#27304,#27305,#27306,#27307),
 .UNSPECIFIED.,.F.,.F.,(4,2,2,2,2,2,2,2,2,2,2,2,2,2,2,2,2,2,2,2,2,2,2,2,
2,2,2,2,2,2,2,2,2,2,2,2,2,2,2,2,2,2,2,2,2,2,2,2,2,2,2,2,2,2,2,2,2,2,2,2,
2,2,2,2,2,2,2,2,2,2,2,2,2,2,2,2,2,2,2,2,2,2,2,2,2,2,2,2,2,2,2,2,2,2,2,2,
2,2,2,2,2,2,2,2,2,2,2,2,2,2,2,2,2,2,2,2,2,2,2,2,2,2,2,2,2,2,2,2,2,2,2,2,
2,2,2,2,2,2,4),(-2.69296972658525,-2.68468620652592,-2.63352519680715,-2.6182365888233,
-2.61011838253823,-2.60879928708178,-2.60811100746982,-2.60755036311805,
-2.60689641371004,-2.60576694829455,-2.60147429737921,-2.59872629691198,
-2.59720788919815,-2.59566566349393,-2.50120186431907,-2.4780487026467,
-2.45373803643959,-2.44905109680547,-2.4478285730644,-2.44685846506811,
-2.44587051189853,-2.44487845943118,-2.4431884798215,-2.43824264444029,
-2.35786091843149,-2.33341673362223,-2.28759442114962,-2.2858703351091,
-2.28510250368146,-2.28453250266342,-2.2839973924358,-2.28325260083479,
-2.28132532815549,-2.25432165401615,-2.16470364356597,-2.13990040469293,
-2.12715509849113,-2.12487339187887,-2.12365553594263,-2.12274813961794,
-2.12175690076819,-2.1200029257124,-2.11484773872556,-2.03124541945865,
-2.01978652501483,-1.96653518848808,-1.96329838690281,-1.96227344424423,
-1.96171189357669,-1.96115053236802,-1.96045052999302,-1.95907512181122,
-1.94947742453603,-1.92527915279096,-1.80913421109112,-1.80310822712246,
-1.80124104596287,-1.80022711855255,-1.79922223566509,-1.79799996208462,
-1.7956969696173,-1.78250668904225,-1.76043456294154,-1.71524525396862,
-1.64429818254088,-1.64025784649695,-1.63915396906366,-1.63850607627418,
-1.63795617911194,-1.63728022051704,-1.63654839176301,-1.63538717231963,
-1.63314907708181,-1.61182682690689,-1.58813702575893,-1.48597514754955,
-1.48000520119616,-1.47814498336495,-1.4771325149925,-1.47612760739122,
-1.47490317346367,-1.47258972709476,-1.45917379146959,-1.45617966016763,
-1.417751180141,-1.32200936824588,-1.31721589594803,-1.31614425704099,-1.31544728125959,
-1.31489881552251,-1.31426988132161,-1.3136038726633,-1.31259948926256,
-1.3107688116457,-1.29565720447254,-1.27595610282393,-1.18645218391262,
-1.15888713637253,-1.15612957322812,-1.15478234103768,-1.15381850215633,
-1.1529033248201,-1.15162331684002,-1.14904229011477,-1.12784712069007,
-1.09276110614157,-1.01015758496455,-0.994982195665562,-0.993444778731139,
-0.992694452782116,-0.992157914440362,-0.991600267651387,-0.990859872937615,
-0.990038966680772,-0.988663745114621,-0.985842831217513,-0.978366231558549,
-0.947222800880595,-0.840039543798158,-0.833793577999617,-0.831900024574466,
-0.830880827702061,-0.829885994805833,-0.828676512595485,-0.826433051695557,
-0.814426316917824,-0.790752097293392,-0.775497557761709,-0.76404449059069,
-0.675783404928685,-0.670986130144879,-0.669914221039829,-0.669217174634,
-0.668688996514639,-0.668066653879922,-0.667027732648787,-0.665779053523944,
-0.663306456513448,-0.661993518361974),.UNSPECIFIED.);
#157=B_SPLINE_CURVE_WITH_KNOTS('',3,(#27312,#27313,#27314,#27315,#27316,
#27317,#27318,#27319,#27320,#27321,#27322,#27323,#27324,#27325,#27326,#27327,
#27328,#27329,#27330,#27331,#27332,#27333,#27334,#27335,#27336,#27337,#27338,
#27339,#27340,#27341,#27342,#27343,#27344,#27345,#27346,#27347,#27348,#27349,
#27350,#27351,#27352,#27353,#27354,#27355,#27356,#27357,#27358,#27359,#27360,
#27361,#27362,#27363,#27364,#27365,#27366,#27367,#27368,#27369,#27370,#27371,
#27372,#27373,#27374,#27375,#27376,#27377,#27378,#27379,#27380,#27381,#27382,
#27383,#27384,#27385,#27386,#27387,#27388,#27389,#27390,#27391,#27392,#27393,
#27394,#27395,#27396,#27397,#27398,#27399,#27400,#27401,#27402,#27403,#27404,
#27405,#27406,#27407,#27408,#27409,#27410,#27411,#27412,#27413,#27414,#27415,
#27416,#27417,#27418,#27419,#27420,#27421,#27422,#27423,#27424,#27425,#27426,
#27427,#27428,#27429,#27430,#27431,#27432,#27433,#27434,#27435,#27436,#27437,
#27438,#27439,#27440,#27441,#27442,#27443,#27444,#27445,#27446,#27447,#27448,
#27449,#27450,#27451,#27452,#27453,#27454,#27455,#27456,#27457,#27458,#27459,
#27460,#27461,#27462,#27463,#27464,#27465,#27466,#27467,#27468,#27469,#27470,
#27471,#27472,#27473,#27474,#27475,#27476,#27477,#27478,#27479,#27480,#27481,
#27482,#27483,#27484,#27485,#27486,#27487,#27488,#27489,#27490,#27491,#27492,
#27493,#27494,#27495,#27496,#27497,#27498,#27499,#27500,#27501,#27502,#27503,
#27504,#27505,#27506,#27507,#27508,#27509,#27510,#27511,#27512,#27513,#27514,
#27515,#27516,#27517,#27518,#27519,#27520,#27521,#27522,#27523,#27524,#27525,
#27526,#27527,#27528,#27529,#27530,#27531,#27532,#27533,#27534,#27535,#27536,
#27537,#27538,#27539,#27540,#27541,#27542,#27543,#27544,#27545,#27546,#27547,
#27548,#27549,#27550,#27551,#27552,#27553,#27554,#27555,#27556,#27557,#27558,
#27559,#27560,#27561,#27562,#27563,#27564,#27565,#27566,#27567,#27568,#27569,
#27570,#27571,#27572,#27573,#27574,#27575,#27576,#27577,#27578,#27579,#27580,
#27581,#27582,#27583,#27584,#27585,#27586,#27587,#27588,#27589,#27590,#27591,
#27592,#27593,#27594,#27595,#27596,#27597,#27598,#27599,#27600,#27601,#27602,
#27603,#27604,#27605,#27606,#27607,#27608,#27609,#27610,#27611,#27612,#27613,
#27614,#27615,#27616,#27617,#27618,#27619,#27620,#27621,#27622,#27623,#27624,
#27625,#27626,#27627,#27628,#27629,#27630,#27631,#27632,#27633,#27634,#27635,
#27636,#27637,#27638,#27639),.UNSPECIFIED.,.F.,.F.,(4,2,2,2,2,2,2,2,2,2,
2,2,2,2,2,2,2,2,2,2,2,2,2,2,2,2,2,2,2,2,2,2,2,2,2,2,2,2,2,2,2,2,2,2,2,2,
2,2,2,2,2,2,2,2,2,2,2,2,2,2,2,2,2,2,2,2,2,2,2,2,2,2,2,2,2,2,2,2,2,2,2,2,
2,2,2,2,2,2,2,2,2,2,2,2,2,2,2,2,2,2,2,2,2,2,2,2,2,2,2,2,2,2,2,2,2,2,2,2,
2,2,2,2,2,2,2,2,2,2,2,2,2,2,2,2,2,2,2,2,2,2,2,2,2,2,2,2,2,2,2,2,2,2,2,2,
2,2,2,2,2,2,2,2,2,4),(-3.4002569369755,-3.38093995940539,-3.37341079928351,
-3.37008548941887,-3.36750340359851,-3.3662285434227,-3.36525601960506,
-3.36428900049934,-3.36292924331676,-3.36011998148307,-3.35252177029656,
-3.35071066604326,-3.34864899011589,-3.34815750990674,-3.34732539752986,
-3.34525421173314,-3.34416589161872,-3.34291406015038,-3.3385200749501,
-3.32571359872987,-3.24124747164086,-3.21009659761013,-3.20589763438741,
-3.20481768677689,-3.20418170915364,-3.20361946518758,-3.20290696255715,
-3.20151596137098,-3.19366591882803,-3.19171327653128,-3.18898195229666,
-3.1272665039378,-3.07498842346378,-3.05634890687441,-3.04982044030199,
-3.04682958654872,-3.04446180850954,-3.04323147190637,-3.0423199323534,
-3.04134703805543,-3.03996587873886,-3.03622444786655,-2.97548396196246,
-2.88655186498026,-2.88283016006228,-2.88179472278712,-2.88116864984802,
-2.88060437268379,-2.87987458188804,-2.8783506817698,-2.86820839051684,
-2.86594505042802,-2.86546547661213,-2.86349671000043,-2.86268981598813,
-2.8595505643578,-2.81731343944554,-2.75442024638738,-2.72749737034993,
-2.7241745247365,-2.72159231182345,-2.72031810304185,-2.71934503212131,
-2.71837733333718,-2.71701560673443,-2.71419898711682,-2.68420888765903,
-2.6068255610027,-2.58369538013232,-2.56793273690783,-2.56035389617473,
-2.55905896442276,-2.55837592846615,-2.55782095464187,-2.55716510355392,
-2.55602688873731,-2.55164248460288,-2.54899972179354,-2.5474772056455,
-2.54629161904587,-2.51528661276665,-2.44232825266544,-2.42642243784693,
-2.40386603522981,-2.40087015809707,-2.39849729139373,-2.39726664838713,
-2.39635494364062,-2.39538189007008,-2.39371840535778,-2.38918472862111,
-2.38341325011321,-2.38227032591378,-2.38088439264233,-2.37894305518372,
-2.37837562470634,-2.37628840720606,-2.37481979235509,-2.37361387204093,
-2.37210375379169,-2.36686026009919,-2.36001768813458,-2.32940600358046,
-2.30747938817261,-2.2608147556054,-2.24021800829072,-2.23691007142292,
-2.23591792270941,-2.2353015473718,-2.23473455926844,-2.23399774126582,
-2.23245362832372,-2.22137477363897,-2.12964916937907,-2.09807296602918,
-2.07816049228507,-2.0756138393405,-2.07434091796376,-2.07342689973637,
-2.07246068343944,-2.07110427940657,-2.0683091308718,-2.03921450140264,
-2.03134310858651,-1.93917165727649,-1.91531810570055,-1.91344486421595,
-1.91270927362096,-1.91217668778318,-1.91160535625868,-1.91082892035555,
-1.9090566328447,-1.87295494700478,-1.78354673816582,-1.75586814299778,
-1.7528013317979,-1.75156511164259,-1.75053608091139,-1.74948244328074,
-1.74794711719066,-1.74391133762156,-1.68918390093871,-1.59594390177468,
-1.59107756364401,-1.59000005870167,-1.58930125992211,-1.58875278979557,
-1.58819081722363,-1.58719764503819,-1.5860163442883,-1.58372488918079,
-1.50003354017457,-1.47220520921794,-1.4667337350966,-1.45456638542023,
-1.4326801241291,-1.42966674982342,-1.42831771091131,-1.42729492657737,
-1.42621188405194,-1.42454018554547,-1.41952611685813,-1.39241695924802,
-1.37023206616483),.UNSPECIFIED.);
#158=B_SPLINE_CURVE_WITH_KNOTS('',3,(#27641,#27642,#27643,#27644,#27645,
#27646,#27647,#27648,#27649,#27650,#27651,#27652,#27653,#27654,#27655,#27656,
#27657,#27658,#27659,#27660,#27661,#27662,#27663,#27664,#27665,#27666,#27667,
#27668,#27669,#27670,#27671,#27672,#27673,#27674,#27675,#27676,#27677,#27678,
#27679,#27680,#27681,#27682,#27683,#27684,#27685,#27686,#27687,#27688,#27689,
#27690,#27691,#27692,#27693,#27694,#27695,#27696,#27697,#27698,#27699,#27700,
#27701,#27702,#27703,#27704,#27705,#27706,#27707,#27708,#27709,#27710,#27711,
#27712,#27713,#27714,#27715,#27716,#27717,#27718,#27719,#27720,#27721,#27722,
#27723,#27724,#27725,#27726,#27727,#27728,#27729,#27730,#27731,#27732,#27733,
#27734,#27735,#27736,#27737,#27738,#27739,#27740,#27741,#27742,#27743,#27744,
#27745,#27746,#27747,#27748,#27749,#27750,#27751,#27752,#27753,#27754,#27755,
#27756),.UNSPECIFIED.,.F.,.F.,(4,2,2,2,2,2,2,2,2,2,2,2,2,2,2,2,2,2,2,2,
2,2,2,2,2,2,2,2,2,2,2,2,2,2,2,2,2,2,2,2,2,2,2,2,2,2,2,2,2,2,2,2,2,2,2,2,
2,4),(-0.661993518361974,-0.657056024906029,-0.64455550155935,-0.631528307324102,
-0.591945605773106,-0.539939346178486,-0.531487654507164,-0.528148183098432,
-0.512107096918439,-0.509475892209214,-0.508185732301801,-0.507174903091217,
-0.506054747920254,-0.504216490000417,-0.497741670140338,-0.456782010869626,
-0.444732500093355,-0.435274402998439,-0.427447812110566,-0.420777149300173,
-0.414980685938955,-0.409870138691596,-0.360774216062856,-0.348778831212832,
-0.347178811475139,-0.346442246396423,-0.345875244647594,-0.34527101670619,
-0.344326148893519,-0.343203655121641,-0.3410677203874,-0.33594243601775,
-0.320357196401774,-0.298962932460557,-0.19388969406574,-0.187752934782705,
-0.185872464077233,-0.184855930337792,-0.183851358010691,-0.182633624223373,
-0.180351526931455,-0.167588943195702,-0.14278596003204,-0.0460035589539252,
-0.0424290591130526,-0.0419995758919044,-0.0401952507269741,-0.0397605070169934,
-0.0375005820256303,-0.0255868872461024,-0.0239899666073891,-0.0232539826081721,
-0.0226870666209287,-0.0221619295362122,-0.0215553304639403,-0.0206945042194828,
-0.0192219951723436,-0.000960706335596301),.UNSPECIFIED.);
#159=B_SPLINE_CURVE_WITH_KNOTS('',3,(#27757,#27758,#27759,#27760,#27761,
#27762,#27763,#27764,#27765,#27766,#27767,#27768,#27769,#27770,#27771,#27772,
#27773,#27774,#27775,#27776,#27777,#27778,#27779,#27780,#27781,#27782,#27783,
#27784,#27785,#27786,#27787,#27788,#27789,#27790,#27791,#27792,#27793,#27794,
#27795,#27796,#27797,#27798,#27799,#27800,#27801,#27802,#27803,#27804,#27805,
#27806,#27807,#27808,#27809,#27810,#27811,#27812,#27813,#27814,#27815,#27816,
#27817,#27818,#27819,#27820,#27821,#27822,#27823,#27824,#27825,#27826,#27827,
#27828,#27829,#27830,#27831,#27832,#27833,#27834,#27835,#27836,#27837,#27838,
#27839,#27840,#27841,#27842,#27843,#27844,#27845,#27846,#27847,#27848,#27849,
#27850,#27851,#27852,#27853,#27854,#27855,#27856,#27857,#27858,#27859,#27860,
#27861,#27862,#27863,#27864,#27865,#27866,#27867,#27868,#27869,#27870,#27871,
#27872,#27873,#27874,#27875,#27876,#27877,#27878,#27879,#27880,#27881,#27882,
#27883,#27884,#27885,#27886,#27887,#27888,#27889,#27890,#27891,#27892,#27893,
#27894,#27895,#27896,#27897,#27898),.UNSPECIFIED.,.F.,.F.,(4,3,3,3,3,3,
3,3,3,3,3,3,3,3,3,3,3,3,3,3,3,3,3,3,3,3,3,3,3,3,3,3,3,3,3,3,3,3,3,3,3,3,
3,3,3,3,3,4),(235.619449019477,235.711588498819,235.803608643581,235.897034026776,
235.988906495499,236.080753124543,236.172599664933,236.267202675985,236.359179201164,
236.455095455154,236.551011709143,236.644084653419,236.737031493056,236.829879864241,
236.922660368896,237.015405691053,237.108140656154,237.200890074495,237.29373871523,
237.386639155842,237.479695051926,237.550726364616,237.643799308892,237.736746148529,
237.829594519714,237.922375024369,238.015120346525,238.107855311627,238.200604729968,
238.293453370703,238.386353811314,238.479409707399,238.550441020089,238.643513964365,
238.736460804002,238.829309175187,238.922089679842,239.014835001998,239.1075699671,
239.200319385441,239.293168026176,239.386068466788,239.479124362872,239.550155675562,
239.643215759794,239.736165073806,239.829009492343,239.856887423777),
 .UNSPECIFIED.);
#160=B_SPLINE_CURVE_WITH_KNOTS('',3,(#27904,#27905,#27906,#27907,#27908,
#27909,#27910,#27911,#27912,#27913,#27914,#27915,#27916,#27917,#27918,#27919,
#27920,#27921,#27922,#27923,#27924,#27925,#27926,#27927,#27928,#27929,#27930,
#27931,#27932,#27933,#27934,#27935,#27936,#27937,#27938,#27939,#27940,#27941,
#27942,#27943,#27944,#27945,#27946,#27947,#27948,#27949,#27950,#27951,#27952,
#27953,#27954,#27955,#27956,#27957,#27958,#27959,#27960,#27961,#27962,#27963,
#27964,#27965,#27966,#27967,#27968,#27969,#27970,#27971,#27972,#27973,#27974,
#27975,#27976,#27977,#27978,#27979,#27980,#27981,#27982,#27983,#27984,#27985,
#27986,#27987,#27988,#27989,#27990,#27991,#27992,#27993,#27994,#27995,#27996,
#27997,#27998,#27999,#28000,#28001,#28002,#28003,#28004,#28005,#28006,#28007,
#28008,#28009,#28010,#28011,#28012,#28013,#28014,#28015,#28016,#28017,#28018,
#28019,#28020,#28021,#28022,#28023,#28024,#28025,#28026,#28027,#28028,#28029,
#28030,#28031,#28032,#28033,#28034,#28035,#28036,#28037,#28038,#28039,#28040,
#28041,#28042,#28043,#28044,#28045,#28046,#28047,#28048,#28049,#28050,#28051,
#28052,#28053,#28054,#28055,#28056,#28057,#28058,#28059,#28060,#28061,#28062,
#28063,#28064,#28065,#28066,#28067,#28068,#28069,#28070,#28071,#28072,#28073,
#28074,#28075,#28076,#28077,#28078,#28079,#28080,#28081,#28082,#28083,#28084,
#28085,#28086,#28087),.UNSPECIFIED.,.F.,.F.,(4,2,2,2,2,2,2,2,2,2,2,2,2,
2,2,2,2,2,2,2,2,2,2,2,2,2,2,2,2,2,2,2,2,2,2,2,2,2,2,2,2,2,2,2,2,2,2,2,2,
2,2,2,2,2,2,2,2,2,2,2,2,2,2,2,2,2,2,2,2,2,2,2,2,2,2,2,2,2,2,2,2,2,2,2,2,
2,2,2,2,2,2,4),(-1.36964518659505,-1.35975521995957,-1.25221247044986,-1.24603872561589,
-1.24415411894559,-1.24313691849069,-1.24214228601081,-1.24095509171357,
-1.23878819228145,-1.23610249248161,-1.18418133570106,-1.0881222005116,
-1.08323509407694,-1.08215611015818,-1.08145694932376,-1.08089586817511,
-1.08025084420382,-1.07913035277394,-1.07444586256288,-1.0545836011284,
-1.03077005348896,-0.944693752867164,-0.942787746443107,-0.941588893058248,
-0.939578726665857,-0.937511240345363,-0.924055961152037,-0.921815410778207,
-0.920481349241073,-0.919461342314697,-0.918394920738009,-0.916858606550287,
-0.912394283568249,-0.905830187262344,-0.887052510767496,-0.839181454072609,
-0.764565146174441,-0.760194084514816,-0.759057295142652,-0.758401839851488,
-0.757846942006245,-0.757163679609985,-0.755867361496471,-0.748254899327575,
-0.732478997414089,-0.685667855198492,-0.630631190666143,-0.602098458404161,
-0.599008170200547,-0.597768149156477,-0.596738189390438,-0.595792210724733,
-0.594370217201789,-0.591018276918166,-0.586425405027232,-0.57480665890243,
-0.549957270598971,-0.522968189632089,-0.448420917945021,-0.437954453149053,
-0.436569588387037,-0.435857850159551,-0.435331463641723,-0.434755492389919,
-0.433952955921809,-0.432030899990704,-0.429382296803235,-0.400754802601841,
-0.361553413704037,-0.342067093199293,-0.315265346544721,-0.279490054839314,
-0.276289555008935,-0.274997477411947,-0.27404817323545,-0.273087522243546,
-0.272090563374284,-0.270785302315558,-0.265101133131289,-0.23845151304283,
-0.219045845906396,-0.124622635263907,-0.122570917098694,-0.114777439237883,
-0.11338936113078,-0.112677364559283,-0.112115021162796,-0.111478389864372,
-0.110396057690462,-0.10617244933288,-0.0746703960157407,-0.000962444157103762),
 .UNSPECIFIED.);
#161=B_SPLINE_CURVE_WITH_KNOTS('',3,(#28088,#28089,#28090,#28091,#28092,
#28093,#28094,#28095,#28096,#28097,#28098,#28099,#28100,#28101,#28102,#28103,
#28104,#28105,#28106,#28107,#28108,#28109,#28110,#28111,#28112,#28113,#28114,
#28115,#28116,#28117,#28118,#28119,#28120,#28121,#28122,#28123,#28124,#28125,
#28126,#28127,#28128,#28129,#28130,#28131,#28132,#28133,#28134,#28135,#28136,
#28137,#28138,#28139,#28140,#28141,#28142,#28143,#28144,#28145,#28146,#28147,
#28148,#28149,#28150,#28151,#28152,#28153,#28154,#28155,#28156,#28157,#28158,
#28159,#28160,#28161,#28162,#28163,#28164,#28165,#28166,#28167,#28168,#28169,
#28170,#28171,#28172,#28173,#28174,#28175,#28176,#28177,#28178,#28179,#28180,
#28181,#28182,#28183,#28184,#28185,#28186,#28187,#28188,#28189),
 .UNSPECIFIED.,.F.,.F.,(4,2,2,2,2,2,2,2,2,2,2,2,2,2,2,2,2,2,2,2,2,2,2,2,
2,2,2,2,2,2,2,2,2,2,2,2,2,2,2,2,2,2,2,2,2,2,2,2,2,2,4),(-4.0614126760776,
-4.01647200025967,-4.0144111607206,-4.0131061350028,-4.01210939553672,-4.01114902005165,
-4.0101999949457,-4.00890840447316,-4.00570965605267,-3.96998663233961,
-3.96536191495626,-3.9595499448839,-3.87547234980412,-3.85483521113081,
-3.85152352851727,-3.85053106586202,-3.84991468297022,-3.84934781966848,
-3.84861134456723,-3.84701116741295,-3.84291310887089,-3.75497311112632,
-3.738950535384,-3.70704022945973,-3.69749140593914,-3.69352252020025,-3.69052237851775,
-3.68945430605423,-3.68851316880395,-3.68749360677421,-3.68616216852436,
-3.68334973942876,-3.66229340280372,-3.65983042983541,-3.6432968181915,
-3.59526136873034,-3.58958945602919,-3.58301287211838,-3.57520788600347,
-3.5655369517722,-3.53009789336455,-3.52820904759051,-3.5274122765838,-3.52683745477759,
-3.52630995777336,-3.52559359698803,-3.5241905155016,-3.51324216205479,
-3.43936917897931,-3.40340392295659,-3.4002569369755),.UNSPECIFIED.);
#162=B_SPLINE_CURVE_WITH_KNOTS('',3,(#28191,#28192,#28193,#28194,#28195,
#28196,#28197,#28198,#28199,#28200,#28201,#28202,#28203,#28204,#28205,#28206,
#28207,#28208,#28209,#28210,#28211,#28212,#28213,#28214,#28215,#28216,#28217,
#28218,#28219,#28220,#28221,#28222,#28223,#28224,#28225,#28226,#28227,#28228,
#28229,#28230,#28231,#28232,#28233,#28234,#28235,#28236,#28237,#28238,#28239,
#28240,#28241,#28242,#28243,#28244,#28245,#28246,#28247,#28248,#28249,#28250,
#28251,#28252,#28253,#28254,#28255,#28256,#28257,#28258,#28259,#28260),
 .UNSPECIFIED.,.F.,.F.,(4,3,3,3,3,3,3,3,3,3,3,3,3,3,3,3,3,3,3,3,3,3,3,4),
(239.856887423777,239.949654754809,240.042394360245,240.135131058889,240.227889660377,
240.320751501073,240.413671838076,240.50673938925,240.549870331035,240.642943275311,
240.735890114948,240.828738486133,240.921518990788,241.014264312944,241.106999278045,
241.199748696387,241.292597337122,241.385497777733,241.478553673818,241.549584986507,
241.656946697205,241.763846790162,241.869934978222,241.902634326219),
 .UNSPECIFIED.);
#163=B_SPLINE_CURVE_WITH_KNOTS('',3,(#28261,#28262,#28263,#28264,#28265,
#28266,#28267,#28268,#28269,#28270,#28271,#28272,#28273,#28274,#28275,#28276,
#28277,#28278,#28279,#28280,#28281,#28282,#28283,#28284,#28285,#28286,#28287,
#28288,#28289,#28290,#28291,#28292,#28293,#28294,#28295,#28296,#28297,#28298,
#28299,#28300,#28301,#28302,#28303,#28304,#28305,#28306,#28307,#28308,#28309,
#28310,#28311,#28312,#28313,#28314,#28315,#28316,#28317,#28318,#28319,#28320,
#28321,#28322,#28323,#28324,#28325,#28326,#28327,#28328,#28329,#28330,#28331,
#28332,#28333,#28334,#28335,#28336,#28337,#28338,#28339,#28340,#28341,#28342,
#28343,#28344,#28345,#28346,#28347,#28348,#28349,#28350,#28351,#28352,#28353,
#28354,#28355,#28356,#28357,#28358,#28359,#28360,#28361,#28362,#28363,#28364,
#28365,#28366,#28367,#28368,#28369,#28370,#28371,#28372,#28373,#28374,#28375,
#28376,#28377,#28378,#28379,#28380,#28381,#28382,#28383,#28384,#28385,#28386,
#28387,#28388,#28389,#28390,#28391,#28392,#28393,#28394,#28395,#28396,#28397,
#28398,#28399,#28400,#28401,#28402,#28403,#28404,#28405,#28406,#28407,#28408,
#28409,#28410,#28411,#28412,#28413,#28414,#28415,#28416,#28417,#28418,#28419,
#28420,#28421,#28422,#28423,#28424,#28425,#28426,#28427,#28428,#28429,#28430,
#28431,#28432,#28433,#28434,#28435,#28436,#28437,#28438,#28439,#28440,#28441,
#28442,#28443,#28444,#28445,#28446,#28447,#28448,#28449,#28450,#28451,#28452,
#28453,#28454,#28455,#28456,#28457,#28458,#28459,#28460,#28461,#28462,#28463,
#28464,#28465,#28466,#28467,#28468,#28469,#28470,#28471,#28472,#28473,#28474,
#28475,#28476,#28477,#28478,#28479,#28480,#28481,#28482,#28483,#28484),
 .UNSPECIFIED.,.F.,.F.,(4,2,2,2,2,2,2,2,2,2,2,2,2,2,2,2,2,2,2,2,2,2,2,2,
2,2,2,2,2,2,2,2,2,2,2,2,2,2,2,2,2,2,2,2,2,2,2,2,2,2,2,2,2,2,2,2,2,2,2,2,
2,2,2,2,2,2,2,2,2,2,2,2,2,2,2,2,2,2,2,2,2,2,2,2,2,2,2,2,2,2,2,2,2,2,2,2,
2,2,2,2,2,2,2,2,2,2,2,2,2,2,2,4),(-4.06280686652475,-4.02033455512575,-4.01828026331028,
-4.01697778898361,-4.01598168379191,-4.01502005815009,-4.01406936210687,
-4.01277240793497,-4.01021522245632,-3.98937646105168,-3.97187848069651,
-3.9661173537507,-3.89668375234783,-3.85664369166857,-3.85489375311297,
-3.85412125783269,-3.85355051365799,-3.85301674460424,-3.85227690920787,
-3.85078183068219,-3.83709118141168,-3.83619183631263,-3.83528921572824,
-3.83383899752311,-3.8322731292852,-3.7529103983421,-3.73382734546682,-3.70906060048441,
-3.69624899056542,-3.69397108344244,-3.69297442645236,-3.69201320003456,
-3.69106311636581,-3.68976854274453,-3.6865545855394,-3.65016425872698,
-3.60234397955488,-3.59686443417707,-3.59056616260913,-3.58318894624673,
-3.55843308008148,-3.53594786162888,-3.53245862649552,-3.53144680872277,
-3.53082595530709,-3.53026019415803,-3.52953221008705,-3.52833383921899,
-3.52173355676252,-3.51997444106321,-3.51898482182036,-3.44233812414972,
-3.40697939713944,-3.38461269742447,-3.37710900162285,-3.37379170851011,
-3.37121417009501,-3.36994010590472,-3.36896674987163,-3.36799871662067,
-3.36663613852138,-3.36381652041266,-3.33371356198764,-3.25484073651609,
-3.24406671242419,-3.22858395719762,-3.21608630485069,-3.20983721983953,
-3.20861077935588,-3.20794235949533,-3.20743759628141,-3.20687258857956,
-3.20583037495989,-3.20245342949653,-3.1465978316981,-3.05847040457446,
-3.05275659812867,-3.05004711352875,-3.04786285490288,-3.04667219649783,
-3.04576513783412,-3.04462833392618,-3.04271571183145,-3.03630850011037,
-3.03237018918773,-3.03064550855694,-3.02802764036341,-3.02756282889643,
-2.93218027663408,-2.88761261626813,-2.88577564572208,-2.88498764372232,
-2.88441419591528,-2.88388433587575,-2.88315945905523,-2.88172374830638,
-2.86987688788731,-2.86909644032182,-2.86869496537234,-2.86771856919629,
-2.86491098912547,-2.82074618689506,-2.7580569001728,-2.73096769952892,
-2.727632340423,-2.72504194653146,-2.72376593754306,-2.72279306223058,-2.72182576120225,
-2.72046611205756,-2.71765870658509,-2.69355746220323),.UNSPECIFIED.);
#164=B_SPLINE_CURVE_WITH_KNOTS('',3,(#28489,#28490,#28491,#28492,#28493,
#28494,#28495,#28496,#28497,#28498,#28499,#28500,#28501,#28502,#28503,#28504,
#28505,#28506,#28507,#28508,#28509,#28510,#28511,#28512,#28513,#28514,#28515,
#28516,#28517,#28518,#28519,#28520,#28521,#28522,#28523,#28524,#28525,#28526,
#28527,#28528,#28529,#28530,#28531,#28532,#28533,#28534,#28535,#28536,#28537,
#28538,#28539,#28540,#28541,#28542,#28543,#28544,#28545,#28546,#28547,#28548,
#28549,#28550,#28551,#28552,#28553,#28554,#28555,#28556,#28557,#28558,#28559,
#28560,#28561,#28562,#28563,#28564,#28565,#28566,#28567,#28568,#28569,#28570,
#28571,#28572,#28573,#28574,#28575,#28576,#28577,#28578,#28579,#28580,#28581,
#28582,#28583,#28584,#28585,#28586,#28587,#28588,#28589,#28590,#28591,#28592,
#28593,#28594,#28595,#28596,#28597,#28598,#28599,#28600,#28601,#28602,#28603,
#28604,#28605,#28606,#28607,#28608,#28609,#28610,#28611,#28612,#28613,#28614,
#28615,#28616,#28617,#28618,#28619,#28620,#28621,#28622,#28623,#28624,#28625,
#28626,#28627,#28628,#28629,#28630,#28631,#28632,#28633,#28634,#28635,#28636,
#28637,#28638,#28639,#28640,#28641,#28642,#28643,#28644,#28645,#28646,#28647,
#28648,#28649,#28650,#28651,#28652,#28653,#28654,#28655,#28656,#28657,#28658,
#28659,#28660,#28661,#28662,#28663,#28664,#28665,#28666,#28667,#28668,#28669,
#28670,#28671,#28672,#28673,#28674,#28675,#28676,#28677,#28678,#28679,#28680,
#28681,#28682,#28683,#28684,#28685,#28686,#28687,#28688,#28689,#28690,#28691,
#28692,#28693,#28694,#28695,#28696,#28697,#28698,#28699,#28700,#28701,#28702,
#28703,#28704,#28705,#28706,#28707,#28708,#28709,#28710,#28711,#28712,#28713,
#28714,#28715,#28716,#28717,#28718,#28719,#28720,#28721,#28722,#28723,#28724,
#28725,#28726,#28727,#28728,#28729,#28730,#28731,#28732,#28733,#28734,#28735,
#28736,#28737,#28738,#28739,#28740,#28741,#28742,#28743,#28744,#28745,#28746,
#28747,#28748,#28749,#28750,#28751,#28752,#28753,#28754,#28755,#28756,#28757,
#28758,#28759,#28760,#28761,#28762,#28763,#28764,#28765,#28766,#28767,#28768,
#28769,#28770,#28771,#28772,#28773,#28774,#28775,#28776,#28777,#28778,#28779,
#28780,#28781,#28782,#28783,#28784,#28785,#28786,#28787,#28788,#28789,#28790,
#28791,#28792,#28793,#28794,#28795,#28796,#28797,#28798,#28799,#28800,#28801,
#28802,#28803,#28804,#28805,#28806,#28807,#28808,#28809,#28810,#28811,#28812,
#28813,#28814,#28815,#28816,#28817,#28818,#28819,#28820,#28821,#28822,#28823,
#28824,#28825,#28826,#28827,#28828,#28829,#28830),.UNSPECIFIED.,.F.,.F.,
(4,2,2,2,2,2,2,2,2,2,2,2,2,2,2,2,2,2,2,2,2,2,2,2,2,2,2,2,2,2,2,2,2,2,2,
2,2,2,2,2,2,2,2,2,2,2,2,2,2,2,2,2,2,2,2,2,2,2,2,2,2,2,2,2,2,2,2,2,2,2,2,
2,2,2,2,2,2,2,2,2,2,2,2,2,2,2,2,2,2,2,2,2,2,2,2,2,2,2,2,2,2,2,2,2,2,2,2,
2,2,2,2,2,2,2,2,2,2,2,2,2,2,2,2,2,2,2,2,2,2,2,2,2,2,2,2,2,2,2,2,2,2,2,2,
2,2,2,2,2,2,2,2,2,2,2,2,2,2,2,2,2,2,2,2,2,2,2,2,2,2,2,4),(-3.39967567881543,
-3.3830953443525,-3.36505840107934,-3.35124254130715,-3.34681003894987,
-3.34394518201433,-3.34323831832382,-3.34257042209722,-3.34206574325176,
-3.34150050644599,-3.34045696262515,-3.3370684895889,-3.28345086884869,
-3.23196100923378,-3.21074239750237,-3.18738545504777,-3.18347741124127,
-3.18194673803801,-3.18089395532038,-3.17986393347204,-3.17862431948622,
-3.17553758177969,-3.14715331885114,-3.13298651681843,-3.12434090791465,
-3.07956953116939,-3.04489480200288,-3.0294959522054,-3.0217081232995,-3.02040717666493,
-3.01971722478535,-3.01921061360912,-3.01865800942075,-3.01767709244384,
-3.01477412252933,-2.96708900932264,-2.8955753256884,-2.87329328342076,
-2.86188973755712,-2.85968533238123,-2.85847452284638,-2.85756792346845,
-2.85642802281662,-2.85450134444521,-2.84797136152875,-2.84409236979748,
-2.84009737720496,-2.83962227563945,-2.83751398695264,-2.83649547778602,
-2.83525627693123,-2.83282249996698,-2.82189256993927,-2.80218570973055,
-2.73266058932669,-2.70844494495866,-2.69885456085533,-2.69748390660192,
-2.69677918901473,-2.69627077366496,-2.69572500543677,-2.69494076929004,
-2.692759130891,-2.65773612233269,-2.57657039176738,-2.55177576204388,-2.53902122466936,
-2.53674608155657,-2.53551987748489,-2.53451480886989,-2.53350326935687,
-2.53164789378162,-2.52571786318746,-2.52426859443777,-2.52070525944668,
-2.51923848221267,-2.51684774587235,-2.51478463134214,-2.51306405552507,
-2.51186176783343,-2.51041499536734,-2.50414798392216,-2.49651832444404,
-2.41126865027625,-2.39815012828021,-2.38292339364967,-2.37565956109738,
-2.37441672858754,-2.37372128087645,-2.3731603308833,-2.37259644404695,
-2.37155964300261,-2.36822656639715,-2.3656046874333,-2.3639455116607,-2.32914627964105,
-2.30881886748014,-2.26924090307963,-2.22231723008055,-2.21772040054798,
-2.21434012995641,-2.21291066925041,-2.21187785023757,-2.21093756139645,
-2.20968185477298,-2.20662384807957,-2.17781148637259,-2.15938127774399,
-2.10393396551719,-2.07893568341549,-2.05581323323315,-2.05346626471223,
-2.05172077953906,-2.05094913177385,-2.05037857006137,-2.04984463929117,
-2.04910407716114,-2.04760595681434,-2.03380957435978,-2.03321213411386,
-2.0327519061593,-2.03138941978545,-2.0310974982289,-2.01059889328218,-1.91962341717732,
-1.91339744935615,-1.91176746808171,-1.91054662736731,-1.90875043988151,
-1.90666967589999,-1.90432937867575,-1.89885659743068,-1.89236855048891,
-1.8904466835123,-1.88930786558113,-1.88840114434487,-1.88718891561229,
-1.88493290446546,-1.87268923043861,-1.84851606945835,-1.80273139451716,
-1.73342268557157,-1.72940430090167,-1.72830270177766,-1.72765534317654,
-1.72709434603407,-1.72639799770446,-1.72503983562958,-1.71592347012686,
-1.69368208996812,-1.57447947769436,-1.56892555173749,-1.56711822683182,
-1.56611649987859,-1.56511053675389,-1.56389249389707,-1.56157776777885,
-1.55867147420948,-1.53726858295719,-1.51515903607891,-1.46439043804796,
-1.40947707420535,-1.40610418846373,-1.40506269379156,-1.40449795680927,
-1.40399336550636,-1.40332507474768,-1.402098570233,-1.39584303416573,-1.38332780208467,
-1.36964518659505),.UNSPECIFIED.);
#165=B_SPLINE_CURVE_WITH_KNOTS('',3,(#28831,#28832,#28833,#28834,#28835,
#28836,#28837,#28838,#28839,#28840,#28841,#28842,#28843,#28844,#28845,#28846,
#28847,#28848,#28849,#28850,#28851,#28852,#28853,#28854,#28855,#28856,#28857,
#28858,#28859,#28860,#28861,#28862,#28863,#28864,#28865,#28866,#28867,#28868,
#28869,#28870,#28871,#28872,#28873,#28874,#28875,#28876,#28877,#28878,#28879,
#28880,#28881,#28882,#28883,#28884,#28885,#28886,#28887,#28888,#28889,#28890,
#28891,#28892,#28893,#28894,#28895,#28896,#28897,#28898,#28899,#28900,#28901,
#28902,#28903,#28904,#28905,#28906,#28907,#28908,#28909,#28910,#28911,#28912,
#28913,#28914,#28915,#28916,#28917,#28918,#28919,#28920,#28921,#28922,#28923,
#28924,#28925,#28926,#28927,#28928,#28929,#28930,#28931,#28932,#28933,#28934,
#28935,#28936,#28937,#28938,#28939,#28940,#28941,#28942,#28943,#28944,#28945,
#28946,#28947,#28948,#28949,#28950,#28951,#28952,#28953,#28954,#28955,#28956,
#28957,#28958,#28959,#28960,#28961,#28962,#28963,#28964,#28965,#28966,#28967,
#28968,#28969,#28970,#28971,#28972,#28973,#28974,#28975,#28976,#28977,#28978,
#28979,#28980,#28981,#28982,#28983,#28984,#28985,#28986,#28987,#28988,#28989,
#28990,#28991,#28992,#28993,#28994,#28995,#28996,#28997,#28998,#28999,#29000,
#29001,#29002,#29003,#29004,#29005,#29006,#29007,#29008,#29009,#29010,#29011,
#29012,#29013,#29014,#29015,#29016,#29017,#29018,#29019,#29020,#29021,#29022,
#29023,#29024,#29025,#29026,#29027,#29028,#29029,#29030,#29031,#29032,#29033,
#29034,#29035,#29036,#29037,#29038,#29039,#29040,#29041,#29042,#29043,#29044,
#29045,#29046,#29047,#29048,#29049,#29050,#29051,#29052,#29053,#29054,#29055,
#29056,#29057,#29058,#29059,#29060,#29061,#29062,#29063,#29064,#29065,#29066,
#29067,#29068,#29069,#29070,#29071,#29072,#29073,#29074,#29075,#29076,#29077,
#29078,#29079,#29080,#29081,#29082,#29083,#29084,#29085,#29086,#29087,#29088,
#29089,#29090,#29091,#29092,#29093,#29094,#29095,#29096,#29097,#29098,#29099,
#29100,#29101,#29102,#29103,#29104,#29105,#29106,#29107,#29108,#29109,#29110,
#29111,#29112,#29113,#29114,#29115,#29116,#29117,#29118,#29119,#29120,#29121,
#29122,#29123,#29124,#29125,#29126,#29127,#29128,#29129,#29130,#29131,#29132),
 .UNSPECIFIED.,.F.,.F.,(4,2,2,2,2,2,2,2,2,2,2,2,2,2,2,2,2,2,2,2,2,2,2,2,
2,2,2,2,2,2,2,2,2,2,2,2,2,2,2,2,2,2,2,2,2,2,2,2,2,2,2,2,2,2,2,2,2,2,2,2,
2,2,2,2,2,2,2,2,2,2,2,2,2,2,2,2,2,2,2,2,2,2,2,2,2,2,2,2,2,2,2,2,2,2,2,2,
2,2,2,2,2,2,2,2,2,2,2,2,2,2,2,2,2,2,2,2,2,2,2,2,2,2,2,2,2,2,2,2,2,2,2,2,
2,2,2,2,2,2,2,2,2,2,2,2,2,2,2,2,2,2,4),(-2.69355746220323,-2.68808306254334,
-2.62719530091855,-2.58710670620264,-2.56655536599016,-2.56325152708279,
-2.56225965768096,-2.56164323541506,-2.56107604888027,-2.5603387592859,
-2.55910913355782,-2.55197717350271,-2.55109710005247,-2.54927839451393,
-2.51932178551233,-2.44684404078419,-2.40936417828723,-2.40531415628346,
-2.40321120527166,-2.40143490616236,-2.40033717294215,-2.39932623264292,
-2.39803595481395,-2.39540459282004,-2.37936419524275,-2.3737100390951,
-2.36230558443699,-2.33611098358868,-2.3179497229805,-2.28412447272664,
-2.25603349973043,-2.24597180476589,-2.24063821455095,-2.23946957510403,
-2.23881377634759,-2.23830960283575,-2.23773573275443,-2.23664951053699,
-2.23289464585289,-2.17257939771721,-2.12376406221615,-2.08255218915795,
-2.07938813241006,-2.07799670224624,-2.07697068689038,-2.07602205082008,
-2.07473314384821,-2.07155188620082,-2.03671642646023,-2.03227512053579,
-1.93099216521922,-1.93050906976677,-1.92819468347773,-1.91809829629106,
-1.91657600068083,-1.91585415134862,-1.91528913463021,-1.9146648421775,
-1.91363810309304,-1.91000597677765,-1.8284814678248,-1.78330370166505,
-1.77894325300126,-1.7772053427426,-1.77600942279755,-1.77280217221968,
-1.77158341580513,-1.76974774863945,-1.76855822077632,-1.76170540018213,
-1.75690003471109,-1.75519567542311,-1.75421426707334,-1.75330453315126,
-1.75206638509156,-1.74968949168405,-1.7348363538769,-1.70160248806689,
-1.5986930804288,-1.59794265375855,-1.59413772848069,-1.59304568146722,
-1.59247049595745,-1.59192115075449,-1.59126215306876,-1.59055402440825,
-1.58944956892835,-1.58736127619187,-1.5352086449426,-1.472686211226,-1.43628958236054,
-1.43307446237775,-1.43177939194847,-1.43082893312545,-1.42980354215728,
-1.42841753832034,-1.42528533507357,-1.37899662759809,-1.32804289250425,
-1.2743199967189,-1.27093233841915,-1.26988856673512,-1.26932309980844,
-1.26877313132404,-1.2680986671437,-1.26736958659043,-1.26621521988017,
-1.26399570538079,-1.24298090419219,-1.22050986619115,-1.11701857741683,
-1.11078839972635,-1.10889615890344,-1.10787691636606,-1.10688157368256,
-1.10567081170219,-1.10342304277453,-1.09134970370977,-1.06753034135642,
-1.02202868496824,-0.963425007183822,-0.96022518209887,-0.948626872810102,
-0.947199581960736,-0.946476768450457,-0.94594736424881,-0.945384821164841,
-0.944620035148599,-0.943762948896898,-0.942299833024079,-0.939231137478979,
-0.930846720530321,-0.905234721674861,-0.815350773001681,-0.809017938289967,
-0.806384931076438,-0.803358502883731,-0.801735783618388,-0.80111608468074,
-0.799073471602111,-0.797001856796111,-0.78845719154436,-0.786356191131843,
-0.785049202922835,-0.784036044018823,-0.782924271235241,-0.781124315072967,
-0.775018514762417,-0.737850470757028,-0.690261267276854,-0.66274989517157),
 .UNSPECIFIED.);
#166=B_SPLINE_CURVE_WITH_KNOTS('',3,(#29138,#29139,#29140,#29141,#29142,
#29143,#29144,#29145,#29146,#29147,#29148,#29149,#29150,#29151,#29152,#29153,
#29154,#29155,#29156,#29157,#29158,#29159,#29160,#29161,#29162,#29163,#29164,
#29165,#29166,#29167,#29168,#29169,#29170,#29171,#29172,#29173,#29174,#29175,
#29176,#29177,#29178,#29179,#29180,#29181,#29182,#29183,#29184,#29185,#29186,
#29187,#29188,#29189,#29190,#29191,#29192,#29193,#29194,#29195,#29196,#29197,
#29198,#29199,#29200,#29201,#29202,#29203,#29204,#29205,#29206,#29207,#29208,
#29209,#29210,#29211,#29212,#29213,#29214,#29215,#29216,#29217,#29218,#29219,
#29220,#29221,#29222,#29223,#29224,#29225,#29226,#29227,#29228,#29229,#29230,
#29231,#29232,#29233,#29234,#29235,#29236,#29237,#29238,#29239,#29240,#29241,
#29242,#29243,#29244,#29245,#29246,#29247,#29248,#29249,#29250,#29251,#29252,
#29253,#29254,#29255,#29256,#29257,#29258,#29259,#29260,#29261,#29262,#29263,
#29264,#29265,#29266,#29267,#29268,#29269,#29270,#29271,#29272,#29273,#29274,
#29275,#29276,#29277,#29278,#29279,#29280,#29281,#29282,#29283,#29284,#29285,
#29286,#29287,#29288,#29289,#29290,#29291,#29292,#29293,#29294,#29295,#29296,
#29297,#29298,#29299,#29300,#29301,#29302,#29303,#29304,#29305,#29306,#29307,
#29308,#29309,#29310,#29311,#29312,#29313,#29314,#29315),.UNSPECIFIED.,
 .F.,.F.,(4,2,2,2,2,2,2,2,2,2,2,2,2,2,2,2,2,2,2,2,2,2,2,2,2,2,2,2,2,2,2,
2,2,2,2,2,2,2,2,2,2,2,2,2,2,2,2,2,2,2,2,2,2,2,2,2,2,2,2,2,2,2,2,2,2,2,2,
2,2,2,2,2,2,2,2,2,2,2,2,2,2,2,2,2,2,2,2,2,4),(-1.36999387029904,-1.36038551158595,
-1.31762389844499,-1.25380100434518,-1.22391567831664,-1.22194538346997,
-1.22119375969203,-1.22065690797706,-1.22014504569075,-1.21941690416308,
-1.21793194522755,-1.20457680034161,-1.1796388353013,-1.12019064637841,
-1.06527158973772,-1.06167038334164,-1.06031142000509,-1.05934442968768,
-1.05843053403945,-1.05715914521277,-1.05469019191152,-1.03684037426563,
-1.01088149984525,-0.95016165050593,-0.902122011800938,-0.899298503146542,
-0.898328561177153,-0.897778168686198,-0.897271054294852,-0.896576618448713,
-0.895254638190057,-0.887698305568242,-0.871918434385414,-0.813991369035933,
-0.743680678251719,-0.739063303907374,-0.737387096331901,-0.736411503145224,
-0.735500551964762,-0.734250553054612,-0.732914455732495,-0.72677599850109,
-0.716915438851108,-0.683146275052802,-0.635827942009692,-0.579873465717165,
-0.576480404111557,-0.575436334007658,-0.574871006961547,-0.574366361840461,
-0.573698673410449,-0.572992097181906,-0.570128194105219,-0.542310602154769,
-0.497010928625636,-0.447298036523179,-0.418567796280074,-0.415512149567664,
-0.414256919163544,-0.413316801673658,-0.412283987369497,-0.41085419677846,
-0.409269047897842,-0.397881355157689,-0.375636457701275,-0.344808510529104,
-0.318708951535554,-0.257246151634893,-0.253628453478827,-0.252557847130535,
-0.251987161400847,-0.251432228617072,-0.25075070803629,-0.250024842406989,
-0.248877826889085,-0.235115973156202,-0.203226660131071,-0.190895198563999,
-0.177895355223375,-0.0983105449797796,-0.0933098889715865,-0.0915778119650202,
-0.0905910739618273,-0.0896829651126328,-0.0884569241156662,-0.0871540150667666,
-0.0850985267796175,-0.0705133346622887,-0.000961684070864306),
 .UNSPECIFIED.);
#167=B_SPLINE_CURVE_WITH_KNOTS('',3,(#29316,#29317,#29318,#29319,#29320,
#29321,#29322,#29323,#29324,#29325,#29326,#29327,#29328,#29329,#29330,#29331,
#29332,#29333,#29334,#29335,#29336,#29337,#29338,#29339,#29340,#29341,#29342,
#29343,#29344,#29345,#29346,#29347,#29348,#29349,#29350,#29351,#29352,#29353,
#29354,#29355,#29356,#29357,#29358,#29359,#29360,#29361,#29362,#29363,#29364,
#29365,#29366,#29367,#29368,#29369,#29370,#29371,#29372,#29373,#29374,#29375,
#29376,#29377,#29378,#29379,#29380,#29381,#29382,#29383,#29384,#29385,#29386,
#29387,#29388,#29389,#29390,#29391,#29392,#29393,#29394,#29395,#29396,#29397,
#29398,#29399,#29400,#29401,#29402,#29403,#29404,#29405,#29406,#29407),
 .UNSPECIFIED.,.F.,.F.,(4,2,2,2,2,2,2,2,2,2,2,2,2,2,2,2,2,2,2,2,2,2,2,2,
2,2,2,2,2,2,2,2,2,2,2,2,2,2,2,2,2,2,2,2,2,4),(-4.06042054730363,-4.0005922877394,
-3.99116121478614,-3.98996052414148,-3.98921216445221,-3.98851447950181,
-3.98795337919572,-3.98730698927864,-3.98620956858338,-3.98223137651607,
-3.91660742706423,-3.9025091505805,-3.88845987089132,-3.84780723330483,
-3.83107095889533,-3.82934432305439,-3.8278132670144,-3.82676039226049,
-3.82573041420785,-3.82449101440008,-3.8214056561052,-3.79307297794185,
-3.74181051804254,-3.7073756672315,-3.67843355687513,-3.66787240049278,
-3.66682003530468,-3.66613390771164,-3.66548081486157,-3.6649767453648,
-3.66440086791002,-3.66330450125364,-3.65945723082002,-3.59730971379012,
-3.54645244330157,-3.51345236418847,-3.50705908331055,-3.50570685660638,
-3.50444516776489,-3.50353259334251,-3.50256173085758,-3.50118864717936,
-3.49749964592874,-3.44158656742523,-3.42639287204158,-3.39967567881543),
 .UNSPECIFIED.);
#168=B_SPLINE_CURVE_WITH_KNOTS('',3,(#29409,#29410,#29411,#29412,#29413,
#29414,#29415,#29416,#29417,#29418,#29419,#29420,#29421,#29422,#29423,#29424,
#29425,#29426,#29427,#29428,#29429,#29430,#29431,#29432,#29433,#29434,#29435,
#29436,#29437,#29438,#29439,#29440,#29441,#29442,#29443,#29444,#29445,#29446,
#29447,#29448,#29449,#29450,#29451,#29452,#29453,#29454,#29455,#29456,#29457,
#29458,#29459,#29460,#29461,#29462,#29463,#29464,#29465,#29466,#29467,#29468,
#29469,#29470,#29471,#29472,#29473,#29474,#29475,#29476,#29477,#29478,#29479,
#29480,#29481,#29482,#29483,#29484,#29485,#29486,#29487,#29488,#29489,#29490,
#29491,#29492,#29493,#29494,#29495,#29496,#29497,#29498),.UNSPECIFIED.,
 .F.,.F.,(4,2,2,2,2,2,2,2,2,2,2,2,2,2,2,2,2,2,2,2,2,2,2,2,2,2,2,2,2,2,2,
2,2,2,2,2,2,2,2,2,2,2,2,2,4),(-0.66274989517157,-0.650332479888293,-0.626028375200515,
-0.624146309993,-0.623409073511506,-0.622875939399027,-0.62231613242395,
-0.621563469297492,-0.620725503751429,-0.619308982368471,-0.616372339296391,
-0.608475599872263,-0.588717528200964,-0.469897195849882,-0.464264192079036,
-0.462446273011553,-0.461442224522316,-0.4604362378638,-0.459196598665069,
-0.45681174857044,-0.441752122397939,-0.407709364426341,-0.36632142642992,
-0.345660776798058,-0.312286497900439,-0.302230681626929,-0.300710540127436,
-0.299989240076922,-0.299441827947265,-0.298916550261646,-0.298020513245856,
-0.295483348160206,-0.291688190419691,-0.280480244061581,-0.262474943293934,
-0.147176473275608,-0.14121527052928,-0.139356235956649,-0.138344066927424,
-0.137339237884532,-0.136114582720796,-0.13379976636545,-0.120350841565661,
-0.106877449195167,-0.0009625259518426),.UNSPECIFIED.);
#169=B_SPLINE_CURVE_WITH_KNOTS('',3,(#29499,#29500,#29501,#29502,#29503,
#29504,#29505,#29506,#29507,#29508,#29509,#29510,#29511,#29512,#29513,#29514,
#29515,#29516,#29517,#29518,#29519,#29520,#29521,#29522,#29523,#29524,#29525,
#29526,#29527,#29528,#29529,#29530,#29531,#29532,#29533,#29534,#29535,#29536,
#29537,#29538,#29539,#29540,#29541,#29542,#29543,#29544,#29545,#29546,#29547,
#29548,#29549,#29550,#29551,#29552,#29553,#29554,#29555,#29556,#29557,#29558,
#29559,#29560,#29561,#29562,#29563,#29564,#29565,#29566,#29567,#29568,#29569,
#29570,#29571,#29572,#29573,#29574,#29575,#29576,#29577,#29578,#29579,#29580,
#29581,#29582,#29583,#29584,#29585,#29586,#29587,#29588,#29589,#29590,#29591,
#29592,#29593,#29594,#29595,#29596,#29597,#29598,#29599,#29600,#29601,#29602,
#29603,#29604,#29605,#29606,#29607,#29608,#29609,#29610,#29611,#29612,#29613,
#29614,#29615,#29616,#29617,#29618,#29619,#29620,#29621,#29622,#29623,#29624,
#29625,#29626,#29627,#29628,#29629,#29630,#29631,#29632,#29633,#29634,#29635,
#29636,#29637,#29638,#29639,#29640),.UNSPECIFIED.,.F.,.F.,(4,3,3,3,3,3,
3,3,3,3,3,3,3,3,3,3,3,3,3,3,3,3,3,3,3,3,3,3,3,3,3,3,3,3,3,3,3,3,3,3,3,3,
3,3,3,3,3,4),(254.469004940774,254.545875507654,254.63894845193,254.731895291567,
254.824743662751,254.917524167407,255.010269489563,255.103004454664,255.195753873006,
255.288602513741,255.381502954352,255.474558850437,255.545590163127,255.638663107403,
255.73160994704,255.824458318225,255.91723882288,256.009984145037,256.102719110138,
256.195468528479,256.288317169214,256.381217609826,256.47427350591,256.5453048186,
256.638377762876,256.731324602513,256.824172973698,256.916953478353,257.00969880051,
257.102433765611,257.195183183952,257.288031824687,257.380932265299,257.473988161383,
257.545019474073,257.638092418349,257.731039257986,257.823887629171,257.916668133826,
258.009413455982,258.102148421083,258.194897839424,258.28774648016,258.380646920771,
258.473702816855,258.544734129546,258.637790900267,258.706503083453),
 .UNSPECIFIED.);
#170=B_SPLINE_CURVE_WITH_KNOTS('',3,(#29645,#29646,#29647,#29648,#29649,
#29650,#29651,#29652,#29653,#29654,#29655,#29656,#29657,#29658,#29659,#29660,
#29661,#29662,#29663,#29664,#29665,#29666,#29667,#29668,#29669,#29670,#29671,
#29672,#29673,#29674,#29675,#29676,#29677,#29678,#29679,#29680,#29681,#29682,
#29683,#29684,#29685,#29686,#29687,#29688,#29689,#29690,#29691,#29692,#29693,
#29694,#29695,#29696,#29697,#29698,#29699,#29700,#29701,#29702,#29703,#29704,
#29705,#29706,#29707,#29708,#29709,#29710,#29711,#29712,#29713,#29714,#29715,
#29716,#29717,#29718,#29719,#29720,#29721,#29722,#29723,#29724,#29725,#29726,
#29727,#29728,#29729,#29730,#29731,#29732,#29733,#29734,#29735,#29736,#29737,
#29738,#29739,#29740,#29741,#29742,#29743,#29744,#29745,#29746,#29747,#29748,
#29749,#29750,#29751,#29752,#29753,#29754,#29755,#29756,#29757,#29758,#29759,
#29760,#29761,#29762,#29763,#29764,#29765,#29766,#29767,#29768,#29769,#29770,
#29771,#29772,#29773,#29774,#29775,#29776,#29777,#29778,#29779,#29780,#29781,
#29782,#29783,#29784,#29785,#29786,#29787,#29788,#29789,#29790,#29791,#29792,
#29793,#29794,#29795,#29796,#29797,#29798,#29799,#29800,#29801,#29802,#29803,
#29804,#29805,#29806,#29807,#29808,#29809,#29810,#29811,#29812,#29813,#29814,
#29815,#29816,#29817,#29818,#29819,#29820,#29821,#29822,#29823,#29824,#29825,
#29826,#29827,#29828,#29829,#29830,#29831,#29832,#29833,#29834,#29835,#29836,
#29837,#29838,#29839,#29840,#29841,#29842,#29843,#29844,#29845,#29846,#29847,
#29848,#29849,#29850,#29851,#29852,#29853,#29854,#29855,#29856,#29857,#29858,
#29859,#29860,#29861,#29862,#29863,#29864,#29865,#29866,#29867,#29868,#29869,
#29870,#29871,#29872,#29873,#29874,#29875,#29876,#29877,#29878,#29879,#29880,
#29881,#29882,#29883,#29884,#29885,#29886,#29887,#29888,#29889,#29890,#29891,
#29892,#29893,#29894,#29895,#29896,#29897,#29898,#29899,#29900,#29901,#29902,
#29903,#29904,#29905,#29906,#29907,#29908,#29909,#29910,#29911,#29912,#29913,
#29914,#29915,#29916,#29917,#29918,#29919,#29920,#29921,#29922,#29923,#29924,
#29925,#29926,#29927,#29928,#29929,#29930,#29931,#29932,#29933,#29934,#29935,
#29936),.UNSPECIFIED.,.F.,.F.,(4,2,2,2,2,2,2,2,2,2,2,2,2,2,2,2,2,2,2,2,
2,2,2,2,2,2,2,2,2,2,2,2,2,2,2,2,2,2,2,2,2,2,2,2,2,2,2,2,2,2,2,2,2,2,2,2,
2,2,2,2,2,2,2,2,2,2,2,2,2,2,2,2,2,2,2,2,2,2,2,2,2,2,2,2,2,2,2,2,2,2,2,2,
2,2,2,2,2,2,2,2,2,2,2,2,2,2,2,2,2,2,2,2,2,2,2,2,2,2,2,2,2,2,2,2,2,2,2,2,
2,2,2,2,2,2,2,2,2,2,2,2,2,2,2,2,2,4),(-3.40020035460252,-3.37286992496302,
-3.33938983808234,-3.32957834964395,-3.32552806993047,-3.32250593341849,
-3.32112261612971,-3.3200980357239,-3.31914748865394,-3.31785100422736,
-3.31529554340392,-3.29450308006559,-3.2841432276615,-3.24474903084824,
-3.20284843490037,-3.17560404763391,-3.16598130893913,-3.16083249817106,
-3.15967897127555,-3.15913505007261,-3.15862603599585,-3.15808203204834,
-3.15714415144621,-3.15454198037331,-3.11289451322465,-3.05353867732869,
-3.01725699256773,-3.0016206479176,-2.99920245977703,-2.9979558462115,-2.99704525874983,
-2.99606805380082,-2.99467183376306,-2.99083453559922,-2.93240477410701,
-2.87519691964922,-2.85503013039824,-2.84373552930794,-2.83794528969366,
-2.83674856143262,-2.83620032910944,-2.83568906211055,-2.83515077738968,
-2.83439394905162,-2.83239224441933,-2.80009786213856,-2.72383646978531,
-2.69693301090561,-2.6787955560365,-2.67627113280134,-2.67500259601845,
-2.67408906614203,-2.67312090198149,-2.6717577334953,-2.6689355739256,-2.6387194190394,
-2.56737060364562,-2.51655752140246,-2.51426870371452,-2.51340942430432,
-2.51281832449685,-2.5122446247344,-2.51155264505258,-2.50982337591692,
-2.4938923087519,-2.40048234513647,-2.36082536469448,-2.35449622612228,
-2.35265922771945,-2.35153940071005,-2.3505285821419,-2.34923804218408,
-2.34660469172915,-2.33051799772303,-2.32736706143738,-2.23331025915569,
-2.20667746912396,-2.19225218253274,-2.19075225018191,-2.19002709632715,
-2.18951565801942,-2.18897768324674,-2.18822205392241,-2.18622746944434,
-2.15451950293483,-2.06903949927627,-2.03677469318652,-2.03118324905011,
-2.0294411490242,-2.02845236386875,-2.027544613661,-2.02632240888829,-2.02401993966408,
-2.01084274740894,-1.98844610656616,-1.94307710785031,-1.87253908005348,
-1.86855205930114,-1.86745368447779,-1.86680705391547,-1.86624594790404,
-1.86554851732254,-1.8641852720124,-1.85493054193059,-1.83212564149997,
-1.73549867441092,-1.7293578678983,-1.72803477100936,-1.72682910529024,
-1.72536177532305,-1.72327480512574,-1.72270859141192,-1.72075203419565,
-1.71933692420312,-1.71584673195347,-1.71442861548772,-1.70835394451707,
-1.70648085120586,-1.70546573810381,-1.70446095523809,-1.70324064220095,
-1.70099263967282,-1.68877521011319,-1.66461607915038,-1.61884322998537,
-1.55572416253681,-1.55400791951182,-1.55274686202051,-1.54788902012261,
-1.5451860328601,-1.54423316117979,-1.54368618724262,-1.54317814961806,
-1.54247625174226,-1.54111899723276,-1.53265096850607,-1.51303160234241,
-1.43383805647339,-1.38788865099564,-1.38451325687428,-1.3831913029516,
-1.38223420269518,-1.38121391678574,-1.37985597799712,-1.37696414030964,
-1.36999387029904),.UNSPECIFIED.);
#171=B_SPLINE_CURVE_WITH_KNOTS('',3,(#29938,#29939,#29940,#29941,#29942,
#29943,#29944,#29945,#29946,#29947,#29948,#29949,#29950,#29951,#29952,#29953,
#29954,#29955,#29956,#29957,#29958,#29959,#29960,#29961,#29962,#29963,#29964,
#29965,#29966,#29967,#29968,#29969,#29970,#29971,#29972,#29973,#29974,#29975,
#29976,#29977,#29978,#29979,#29980,#29981,#29982,#29983,#29984,#29985,#29986,
#29987,#29988,#29989,#29990,#29991,#29992,#29993,#29994,#29995,#29996,#29997,
#29998,#29999,#30000,#30001,#30002,#30003,#30004),.UNSPECIFIED.,.F.,.F.,
(4,3,3,3,3,3,3,3,3,3,3,3,3,3,3,3,3,3,3,3,3,3,4),(258.706503083453,258.799374498467,
258.892508784286,258.985260787678,259.077996047084,259.170739374796,259.264166727352,
259.357052077616,259.450750431317,259.544448785018,259.637521729293,259.730468568931,
259.823316940115,259.916097444771,260.008842766927,260.101577732028,260.194327150369,
260.287175791104,260.380076231715,260.4731321278,260.544163440491,260.67516406308,
260.752190247954),.UNSPECIFIED.);
#172=B_SPLINE_CURVE_WITH_KNOTS('',3,(#30005,#30006,#30007,#30008,#30009,
#30010,#30011,#30012,#30013,#30014,#30015,#30016,#30017,#30018,#30019,#30020,
#30021,#30022,#30023,#30024,#30025,#30026,#30027,#30028,#30029,#30030,#30031,
#30032,#30033,#30034,#30035,#30036,#30037,#30038,#30039,#30040,#30041,#30042,
#30043,#30044,#30045,#30046,#30047,#30048,#30049,#30050,#30051,#30052,#30053,
#30054,#30055,#30056,#30057,#30058,#30059,#30060,#30061,#30062,#30063,#30064,
#30065,#30066,#30067,#30068,#30069,#30070,#30071,#30072,#30073,#30074,#30075,
#30076,#30077,#30078,#30079,#30080,#30081,#30082,#30083,#30084,#30085,#30086,
#30087,#30088,#30089,#30090,#30091,#30092,#30093,#30094,#30095,#30096,#30097,
#30098,#30099,#30100,#30101,#30102,#30103,#30104,#30105,#30106,#30107,#30108,
#30109,#30110,#30111,#30112,#30113,#30114,#30115,#30116,#30117,#30118,#30119,
#30120,#30121,#30122,#30123,#30124,#30125,#30126,#30127,#30128,#30129,#30130,
#30131,#30132,#30133,#30134,#30135,#30136,#30137,#30138,#30139,#30140,#30141,
#30142,#30143,#30144,#30145,#30146,#30147,#30148,#30149,#30150,#30151,#30152,
#30153,#30154,#30155,#30156,#30157,#30158,#30159,#30160,#30161,#30162,#30163,
#30164,#30165,#30166,#30167,#30168,#30169,#30170,#30171,#30172,#30173,#30174,
#30175,#30176,#30177,#30178,#30179,#30180,#30181,#30182,#30183,#30184,#30185,
#30186,#30187,#30188,#30189,#30190,#30191,#30192,#30193,#30194,#30195,#30196,
#30197,#30198),.UNSPECIFIED.,.F.,.F.,(4,2,2,2,2,2,2,2,2,2,2,2,2,2,2,2,2,
2,2,2,2,2,2,2,2,2,2,2,2,2,2,2,2,2,2,2,2,2,2,2,2,2,2,2,2,2,2,2,2,2,2,2,2,
2,2,2,2,2,2,2,2,2,2,2,2,2,2,2,2,2,2,2,2,2,2,2,2,2,2,2,2,2,2,2,2,2,2,2,2,
2,2,2,2,2,2,2,4),(-4.06112921706716,-3.99952851532468,-3.98053447412182,
-3.97391345062148,-3.97089124990811,-3.96848146199215,-3.96723691515219,
-3.96624018267477,-3.96524186186338,-3.9634510376057,-3.9580211956521,-3.87425784785127,
-3.86206194772413,-3.85077444982639,-3.82185557989671,-3.80804043109872,
-3.80686960787162,-3.80613384473297,-3.80544527476301,-3.80488493760528,
-3.80431743320141,-3.80326202539012,-3.79977270101839,-3.74333468066042,
-3.7162653577986,-3.6853947360215,-3.66060802632784,-3.64785124553421,-3.64555785575898,
-3.64433783035865,-3.64343056503086,-3.6424411919896,-3.64069509869915,
-3.63559270803827,-3.55540863638263,-3.51261763606852,-3.48547780529754,
-3.48363903037883,-3.48300731859009,-3.48239252526604,-3.48182513114613,
-3.48108521897648,-3.47984613987233,-3.4725385975809,-3.47188518929711,
-3.47002180672503,-3.42594428605793,-3.37659622176019,-3.34071141219027,
-3.33047470238178,-3.32415600101936,-3.32280853346351,-3.32155036292091,
-3.32063847397662,-3.31966659723736,-3.31800853348013,-3.31350931295932,
-3.24048713832828,-3.1851290131769,-3.16941407347762,-3.16170814242443,
-3.16041120950007,-3.15972220444836,-3.15921578592962,-3.15866289018175,
-3.15785284878809,-3.15549635783017,-3.11445846781135,-3.05953304842109,
-3.01909050397777,-3.00236679610937,-2.99992982363778,-2.99866854606279,
-2.99775619567953,-2.99678550284927,-2.99541254557325,-2.99172321742471,
-2.93580968400112,-2.88036834265004,-2.86029346088551,-2.84138581136272,
-2.83826297786502,-2.83729155482927,-2.83667540460607,-2.83610840962103,
-2.83537128833854,-2.83376784259632,-2.82167583971944,-2.81965157443225,
-2.81924525341923,-2.81748741743982,-2.81640948552166,-2.81480242289232,
-2.8039779214992,-2.73415234090667,-2.69567812464718,-2.69249402637897),
 .UNSPECIFIED.);
#173=B_SPLINE_CURVE_WITH_KNOTS('',3,(#30204,#30205,#30206,#30207,#30208,
#30209,#30210,#30211,#30212,#30213,#30214,#30215,#30216,#30217,#30218,#30219,
#30220,#30221,#30222,#30223,#30224,#30225,#30226,#30227,#30228,#30229,#30230,
#30231,#30232,#30233,#30234,#30235,#30236,#30237,#30238,#30239,#30240,#30241,
#30242,#30243,#30244,#30245,#30246,#30247,#30248,#30249,#30250,#30251,#30252,
#30253,#30254,#30255,#30256,#30257,#30258,#30259,#30260,#30261,#30262,#30263,
#30264,#30265,#30266,#30267,#30268,#30269,#30270,#30271,#30272,#30273,#30274,
#30275,#30276,#30277,#30278,#30279,#30280,#30281,#30282,#30283,#30284,#30285,
#30286,#30287,#30288,#30289,#30290,#30291,#30292,#30293,#30294,#30295,#30296,
#30297,#30298,#30299,#30300,#30301,#30302,#30303,#30304,#30305,#30306,#30307,
#30308,#30309,#30310,#30311,#30312,#30313,#30314,#30315,#30316,#30317,#30318,
#30319,#30320,#30321,#30322,#30323,#30324,#30325,#30326,#30327,#30328,#30329,
#30330,#30331,#30332,#30333,#30334,#30335,#30336,#30337,#30338,#30339,#30340,
#30341,#30342,#30343,#30344,#30345,#30346,#30347,#30348,#30349,#30350,#30351,
#30352,#30353,#30354,#30355,#30356,#30357,#30358,#30359,#30360,#30361,#30362,
#30363,#30364,#30365,#30366,#30367,#30368,#30369,#30370,#30371,#30372,#30373,
#30374,#30375,#30376,#30377,#30378,#30379,#30380,#30381,#30382,#30383,#30384,
#30385,#30386,#30387,#30388,#30389,#30390,#30391,#30392,#30393,#30394,#30395,
#30396,#30397,#30398,#30399,#30400,#30401,#30402,#30403),.UNSPECIFIED.,
 .F.,.F.,(4,2,2,2,2,2,2,2,2,2,2,2,2,2,2,2,2,2,2,2,2,2,2,2,2,2,2,2,2,2,2,
2,2,2,2,2,2,2,2,2,2,2,2,2,2,2,2,2,2,2,2,2,2,2,2,2,2,2,2,2,2,2,2,2,2,2,2,
2,2,2,2,2,2,2,2,2,2,2,2,2,2,2,2,2,2,2,2,2,2,2,2,2,2,2,2,2,2,2,2,4),(-1.3693964092334,
-1.36183439143161,-1.36010319153898,-1.35941094504259,-1.35883722412521,
-1.35824631706058,-1.35738774872029,-1.35510335019303,-1.30469303630108,
-1.2448958121231,-1.2284289213657,-1.22211036730221,-1.21833670807719,-1.20208421397686,
-1.19944273305659,-1.19815058222417,-1.19713958817945,-1.19602067894988,
-1.19418771517626,-1.18789162911997,-1.14857759964781,-1.0805957109202,
-1.06483799454862,-1.03920499263226,-1.03730055369081,-1.03655966834246,
-1.0360256769157,-1.03545521873882,-1.03489280902372,-1.03356034031026,
-1.02501038137103,-1.00519442111407,-0.94854448356068,-0.902992456867276,
-0.900523872630309,-0.87947565454661,-0.876662910235612,-0.875331177247815,
-0.874311325157472,-0.873221519279924,-0.871519114858775,-0.866378945849957,
-0.842713618877838,-0.819747677814011,-0.76675100800911,-0.717581830234194,
-0.714718787904132,-0.713742997986063,-0.713191423705019,-0.712684578634125,
-0.711992547399501,-0.710681876017459,-0.702665426873464,-0.697023549330324,
-0.672461574805865,-0.633638711634387,-0.559398272293452,-0.558836508289221,
-0.554416477653384,-0.552770375573333,-0.551800710323614,-0.550887775478914,
-0.549623245088429,-0.548267054066933,-0.541809770541231,-0.506611221790919,
-0.498859904550877,-0.451990904665234,-0.395415657720684,-0.39191541499804,
-0.390858499559347,-0.390290571184745,-0.389730064843355,-0.389041648668859,
-0.388306182843127,-0.3850435462767,-0.379798867627013,-0.367932205113843,
-0.341137085985596,-0.318131079871123,-0.236913392853596,-0.23168252000432,
-0.229918188753276,-0.228924982149571,-0.228018130382196,-0.226804469889529,
-0.224541768058863,-0.212405067709946,-0.143914481944666,-0.132434716809599,
-0.0815972688082654,-0.0698091558616626,-0.0683756690717537,-0.0676514255875008,
-0.0671217931249414,-0.066548354386866,-0.0659805484161044,-0.0652189038625169,
-0.0639864071546979,-0.000961292996707948),.UNSPECIFIED.);
#174=B_SPLINE_CURVE_WITH_KNOTS('',3,(#30404,#30405,#30406,#30407,#30408,
#30409,#30410,#30411,#30412,#30413,#30414,#30415,#30416,#30417,#30418,#30419,
#30420,#30421,#30422,#30423,#30424,#30425,#30426,#30427,#30428,#30429,#30430,
#30431,#30432,#30433,#30434,#30435,#30436,#30437,#30438,#30439,#30440,#30441,
#30442,#30443,#30444,#30445,#30446,#30447,#30448,#30449,#30450,#30451,#30452,
#30453,#30454,#30455,#30456,#30457,#30458,#30459,#30460,#30461,#30462,#30463,
#30464,#30465,#30466,#30467,#30468,#30469,#30470,#30471,#30472,#30473,#30474,
#30475,#30476,#30477,#30478,#30479,#30480,#30481,#30482,#30483,#30484,#30485,
#30486,#30487,#30488,#30489,#30490,#30491,#30492,#30493,#30494,#30495,#30496,
#30497),.UNSPECIFIED.,.F.,.F.,(4,2,2,2,2,2,2,2,2,2,2,2,2,2,2,2,2,2,2,2,
2,2,2,2,2,2,2,2,2,2,2,2,2,2,2,2,2,2,2,2,2,2,2,2,2,2,4),(-4.06159336205859,
-3.99887010139295,-3.98005278788117,-3.973477430799,-3.97047047861041,-3.96807041057785,
-3.96682765673153,-3.96583078164577,-3.96483099104849,-3.96303389041738,
-3.95755932108663,-3.87303910799899,-3.86092619524348,-3.84976664354091,
-3.8211125343086,-3.80741249455709,-3.80630786437716,-3.80559979486472,
-3.80493103976298,-3.80442631822024,-3.80386166428903,-3.80282096307824,
-3.79945572828611,-3.74364984006477,-3.71603882454403,-3.68438630978772,
-3.65978046623324,-3.64729849982294,-3.64501824938511,-3.64380079053548,
-3.64289352602596,-3.64190226898059,-3.64014782893529,-3.63498832635877,
-3.55437381501121,-3.51385549988604,-3.49547979083049,-3.48419226853867,
-3.4827699658635,-3.48219787328426,-3.48162195136153,-3.48109526778725,
-3.48038263679504,-3.47899459597122,-3.46845176566513,-3.42568150182095,
-3.40020035460252),.UNSPECIFIED.);
#175=B_SPLINE_CURVE_WITH_KNOTS('',3,(#30498,#30499,#30500,#30501,#30502,
#30503,#30504,#30505,#30506,#30507,#30508,#30509,#30510,#30511,#30512,#30513,
#30514,#30515,#30516,#30517,#30518,#30519,#30520,#30521,#30522,#30523,#30524,
#30525,#30526,#30527,#30528,#30529,#30530,#30531,#30532,#30533,#30534,#30535,
#30536,#30537,#30538,#30539,#30540,#30541,#30542,#30543,#30544,#30545,#30546,
#30547,#30548,#30549,#30550,#30551,#30552,#30553,#30554,#30555,#30556,#30557,
#30558,#30559,#30560,#30561,#30562,#30563,#30564,#30565,#30566,#30567,#30568,
#30569,#30570,#30571,#30572,#30573,#30574,#30575,#30576,#30577,#30578,#30579,
#30580,#30581,#30582,#30583,#30584,#30585,#30586,#30587,#30588,#30589,#30590,
#30591,#30592,#30593,#30594,#30595,#30596,#30597,#30598,#30599,#30600,#30601,
#30602,#30603,#30604,#30605,#30606,#30607,#30608,#30609,#30610,#30611,#30612,
#30613,#30614,#30615,#30616,#30617,#30618,#30619,#30620,#30621,#30622,#30623,
#30624,#30625,#30626,#30627,#30628,#30629,#30630,#30631,#30632,#30633,#30634,
#30635,#30636,#30637,#30638,#30639,#30640,#30641,#30642,#30643,#30644,#30645,
#30646,#30647,#30648,#30649,#30650,#30651,#30652,#30653,#30654,#30655,#30656,
#30657,#30658,#30659,#30660,#30661,#30662,#30663,#30664,#30665,#30666,#30667,
#30668,#30669,#30670,#30671,#30672,#30673,#30674,#30675,#30676,#30677,#30678,
#30679,#30680,#30681,#30682,#30683,#30684,#30685,#30686,#30687,#30688,#30689,
#30690,#30691,#30692,#30693,#30694,#30695,#30696,#30697,#30698,#30699,#30700,
#30701,#30702,#30703,#30704,#30705,#30706,#30707,#30708,#30709,#30710,#30711,
#30712,#30713,#30714,#30715,#30716,#30717,#30718,#30719,#30720,#30721,#30722,
#30723,#30724,#30725,#30726,#30727,#30728,#30729,#30730,#30731,#30732,#30733,
#30734,#30735,#30736,#30737,#30738,#30739,#30740,#30741,#30742,#30743,#30744,
#30745,#30746,#30747,#30748,#30749,#30750,#30751,#30752,#30753,#30754,#30755,
#30756,#30757,#30758,#30759,#30760,#30761,#30762,#30763,#30764,#30765,#30766,
#30767,#30768,#30769,#30770,#30771,#30772,#30773,#30774,#30775,#30776,#30777,
#30778,#30779,#30780,#30781,#30782,#30783,#30784,#30785,#30786,#30787,#30788,
#30789,#30790,#30791,#30792,#30793,#30794,#30795,#30796,#30797,#30798,#30799,
#30800,#30801,#30802,#30803,#30804,#30805,#30806,#30807,#30808,#30809),
 .UNSPECIFIED.,.F.,.F.,(4,2,2,2,2,2,2,2,2,2,2,2,2,2,2,2,2,2,2,2,2,2,2,2,
2,2,2,2,2,2,2,2,2,2,2,2,2,2,2,2,2,2,2,2,2,2,2,2,2,2,2,2,2,2,2,2,2,2,2,2,
2,2,2,2,2,2,2,2,2,2,2,2,2,2,2,2,2,2,2,2,2,2,2,2,2,2,2,2,2,2,2,2,2,2,2,2,
2,2,2,2,2,2,2,2,2,2,2,2,2,2,2,2,2,2,2,2,2,2,2,2,2,2,2,2,2,2,2,2,2,2,2,2,
2,2,2,2,2,2,2,2,2,2,2,2,2,2,2,2,2,2,2,2,2,2,2,4),(-2.69249402637897,-2.67946463668276,
-2.67702422137398,-2.67577316515414,-2.67486219303942,-2.67388728734497,
-2.67249889944679,-2.66871122340817,-2.60799749771988,-2.5191478792325,
-2.51666595625057,-2.5148539143885,-2.514072506601,-2.51349743250879,-2.51296989519231,
-2.51225375602772,-2.51085192768008,-2.49994450458902,-2.45516160274233,
-2.36281457493466,-2.35547737922528,-2.35354318286739,-2.35240169304034,
-2.35139471732816,-2.3501401917013,-2.34820843898228,-2.33949521373088,
-2.33728128680638,-2.3352569798727,-2.3345927468463,-2.33300804766535,-2.32853492723566,
-2.3119192632956,-2.24880265539618,-2.1960242694092,-2.19236410575416,-2.19133482478078,
-2.19071013711643,-2.19014553700179,-2.18942525122613,-2.18791004194552,
-2.17796017589408,-2.08659169317583,-2.03433773191786,-2.03126820599149,
-2.03003159948487,-2.02900252786405,-2.02794913534297,-2.02641469068709,
-2.0223841989686,-1.96793370091752,-1.8743455635147,-1.86955292834131,-1.86848141873188,
-1.86778451662508,-1.8672235053693,-1.86657661277041,-1.86544803535368,
-1.86066185269588,-1.80582898886298,-1.7396880423071,-1.71132372305559,
-1.70823769455867,-1.70699825658492,-1.70596833654851,-1.70491561382164,
-1.70338494768895,-1.69946965522598,-1.64986819289321,-1.56382885985272,
-1.56291518796767,-1.56029950838556,-1.5598038218094,-1.55898482240542,
-1.54718683955472,-1.54575292810751,-1.54502854694235,-1.54449885061102,
-1.54392537957018,-1.54315289457259,-1.54139183153711,-1.53899621999878,
-1.45747679823816,-1.41229425846852,-1.40799722915126,-1.40595104425385,
-1.40474598873148,-1.40323814151953,-1.40115695618339,-1.40053504869551,
-1.39921573186698,-1.39874974815342,-1.39752938877203,-1.39435920412947,
-1.38659930565743,-1.38456655308647,-1.38339080697997,-1.38239594189719,
-1.38118943855668,-1.37900484029176,-1.36794577688663,-1.3465228297865,
-1.30415819221214,-1.24047784010733,-1.23835859953043,-1.23617267173459,
-1.23415843269291,-1.22408171676777,-1.22256058618864,-1.22183907500437,
-1.22127422706386,-1.2206500194128,-1.21964378153587,-1.21621048399678,
-1.13281131416596,-1.09660634635944,-1.08978248178416,-1.08434638888271,
-1.08295171041495,-1.08174625091998,-1.08026302207705,-1.07817838664266,
-1.0775920382433,-1.07589779111494,-1.07495263438374,-1.07222771756648,
-1.06373154765066,-1.06181731377792,-1.06056813295458,-1.05956144238387,
-1.05841593713943,-1.05650332789887,-1.04922580395954,-1.01622776644239,
-0.951273214040969,-0.902952901245586,-0.900119869414113,-0.899148424568292,
-0.898597701395266,-0.898090615477028,-0.897396718877762,-0.896077428880517,
-0.887858070659571,-0.87034158846105,-0.813649386766575,-0.744323227927764,
-0.739839795904135,-0.738183876341585,-0.737212241251194,-0.736299922102091,
-0.735040127441836,-0.733690509118304,-0.727342204009417,-0.717043392512378,
-0.680814601167412,-0.662293107873676),.UNSPECIFIED.);
#176=B_SPLINE_CURVE_WITH_KNOTS('',3,(#30814,#30815,#30816,#30817,#30818,
#30819,#30820,#30821,#30822,#30823,#30824,#30825,#30826,#30827,#30828,#30829,
#30830,#30831,#30832,#30833,#30834,#30835,#30836,#30837,#30838,#30839,#30840,
#30841,#30842,#30843,#30844,#30845,#30846,#30847,#30848,#30849,#30850,#30851,
#30852,#30853,#30854,#30855,#30856,#30857,#30858,#30859,#30860,#30861,#30862,
#30863,#30864,#30865,#30866,#30867,#30868,#30869,#30870,#30871,#30872,#30873,
#30874,#30875,#30876,#30877,#30878,#30879,#30880,#30881,#30882,#30883,#30884,
#30885,#30886,#30887,#30888,#30889,#30890,#30891,#30892,#30893,#30894,#30895,
#30896,#30897,#30898,#30899,#30900,#30901,#30902,#30903,#30904,#30905,#30906,
#30907,#30908,#30909,#30910,#30911,#30912,#30913,#30914,#30915,#30916,#30917,
#30918,#30919,#30920,#30921,#30922,#30923,#30924,#30925,#30926,#30927,#30928,
#30929,#30930,#30931,#30932,#30933,#30934,#30935,#30936,#30937,#30938,#30939,
#30940,#30941,#30942,#30943,#30944,#30945,#30946,#30947,#30948,#30949,#30950,
#30951,#30952,#30953,#30954,#30955,#30956,#30957,#30958,#30959,#30960,#30961,
#30962,#30963,#30964,#30965,#30966,#30967,#30968,#30969,#30970,#30971,#30972,
#30973,#30974,#30975,#30976,#30977,#30978,#30979,#30980,#30981,#30982,#30983,
#30984,#30985,#30986,#30987,#30988,#30989,#30990,#30991,#30992,#30993,#30994,
#30995,#30996,#30997,#30998,#30999,#31000,#31001,#31002,#31003,#31004,#31005,
#31006,#31007,#31008,#31009,#31010,#31011,#31012,#31013,#31014,#31015,#31016,
#31017,#31018,#31019,#31020,#31021,#31022,#31023,#31024,#31025,#31026,#31027,
#31028,#31029,#31030,#31031,#31032,#31033,#31034,#31035,#31036,#31037,#31038,
#31039,#31040,#31041,#31042,#31043,#31044,#31045,#31046,#31047,#31048,#31049,
#31050,#31051,#31052,#31053,#31054,#31055,#31056,#31057,#31058,#31059,#31060,
#31061,#31062,#31063,#31064,#31065,#31066,#31067,#31068,#31069,#31070,#31071,
#31072,#31073,#31074,#31075,#31076,#31077),.UNSPECIFIED.,.F.,.F.,(4,2,2,
2,2,2,2,2,2,2,2,2,2,2,2,2,2,2,2,2,2,2,2,2,2,2,2,2,2,2,2,2,2,2,2,2,2,2,2,
2,2,2,2,2,2,2,2,2,2,2,2,2,2,2,2,2,2,2,2,2,2,2,2,2,2,2,2,2,2,2,2,2,2,2,2,
2,2,2,2,2,2,2,2,2,2,2,2,2,2,2,2,2,2,2,2,2,2,2,2,2,2,2,2,2,2,2,2,2,2,2,2,
2,2,2,2,2,2,2,2,2,2,2,2,2,2,2,2,2,2,2,2,4),(-3.39927600084928,-3.37983339994959,
-3.34294734504984,-3.31433754663311,-3.30418735458775,-3.29882030444007,
-3.29764984383165,-3.29699388183311,-3.29648999236438,-3.2959168839376,
-3.29483339945536,-3.29109948697606,-3.29025532320103,-3.21490936905459,
-3.16755329055488,-3.14905012806519,-3.14255781321543,-3.13957945591476,
-3.13721882384085,-3.13599073195639,-3.13500037271095,-3.1338642541134,
-3.13195298730607,-3.12555202678434,-3.12161458651954,-3.12020473076913,
-3.11935000604415,-3.01984423732388,-2.98039665705453,-2.97575814675145,
-2.97464139795801,-2.97399725493184,-2.973436157739,-2.97273596942656,-2.97165353768983,
-2.96672206909679,-2.87137035732331,-2.82010506282366,-2.81682148915416,
-2.81426671493517,-2.81299700275787,-2.8120047868187,-2.81103160777165,
-2.80936629754912,-2.80481828421088,-2.73111340778257,-2.68256256963272,
-2.66190940206984,-2.65317197193653,-2.65182849917876,-2.65113539101577,
-2.65062860361498,-2.65007792907969,-2.64910586928944,-2.64626693994028,
-2.59782986577639,-2.52715242147492,-2.49979581152239,-2.49517749171423,
-2.49286236629535,-2.49145066566343,-2.4901642771863,-2.48916945831023,
-2.48820307448141,-2.48684546159887,-2.48404467661298,-2.45469282491939,
-2.36670907214967,-2.35346793164522,-2.33293593130824,-2.32963464118569,
-2.3286433758527,-2.32802729163341,-2.32746039005114,-2.32672343564521,
-2.32517815358206,-2.31406380224303,-2.22071699463133,-2.19035163301207,
-2.17089613266334,-2.16836285217489,-2.16709284088173,-2.16617942405667,
-2.16521246745381,-2.16385277770752,-2.16104358893022,-2.13134048927929,
-2.04365628199531,-2.03042309445068,-2.01940389077499,-2.00766771637792,
-2.0060982465228,-2.00535640695997,-2.00478873437102,-2.0041748636839,-2.0031935221447,
-1.99998089796753,-1.95154853065194,-1.90179336369731,-1.84947307008481,
-1.8460211363495,-1.84468665128501,-1.84372639110705,-1.84270820287488,
-1.84136232043809,-1.83844332240344,-1.79228637482434,-1.68759240910398,
-1.68380751800067,-1.68271808456167,-1.6821436354163,-1.68163957939732,
-1.68098479851308,-1.67987833338735,-1.67514345594757,-1.63265139736368,
-1.55223836542906,-1.54527219738183,-1.54377274317074,-1.54257783707578,
-1.53879692162831,-1.53838448508005,-1.52482418715018,-1.52257779404412,
-1.52124190185589,-1.52022145830609,-1.51913353482445,-1.51743925095977,
-1.51234770027879,-1.45206474110987,-1.37783960546454,-1.3693964092334),
 .UNSPECIFIED.);
#177=B_SPLINE_CURVE_WITH_KNOTS('',3,(#31079,#31080,#31081,#31082,#31083,
#31084,#31085,#31086,#31087,#31088,#31089,#31090,#31091,#31092,#31093,#31094,
#31095,#31096,#31097,#31098,#31099,#31100,#31101,#31102,#31103,#31104,#31105,
#31106,#31107,#31108,#31109,#31110,#31111,#31112,#31113,#31114,#31115,#31116,
#31117,#31118,#31119,#31120,#31121,#31122,#31123,#31124,#31125,#31126,#31127,
#31128,#31129,#31130,#31131,#31132,#31133,#31134,#31135,#31136,#31137,#31138,
#31139,#31140,#31141,#31142,#31143,#31144,#31145,#31146,#31147,#31148,#31149,
#31150,#31151,#31152,#31153,#31154,#31155,#31156,#31157,#31158,#31159,#31160,
#31161,#31162,#31163,#31164,#31165,#31166,#31167,#31168,#31169,#31170,#31171,
#31172,#31173,#31174,#31175,#31176),.UNSPECIFIED.,.F.,.F.,(4,2,2,2,2,2,
2,2,2,2,2,2,2,2,2,2,2,2,2,2,2,2,2,2,2,2,2,2,2,2,2,2,2,2,2,2,2,2,2,2,2,2,
2,2,2,2,2,2,4),(-0.662293107873676,-0.63546222695704,-0.624451999974867,
-0.57998846595183,-0.577166231313401,-0.576196463240149,-0.575646089194518,
-0.575138940377343,-0.57444437948297,-0.573700372012397,-0.570306893612535,
-0.54328226613345,-0.498543488887952,-0.446538136168641,-0.438044811829723,
-0.434725077017795,-0.418691546503556,-0.416060707706702,-0.414770615999668,
-0.413759789163189,-0.412639584224645,-0.410801125156248,-0.404460584912384,
-0.394177663305687,-0.35803734504289,-0.337988470814761,-0.317499512253371,
-0.257902129752157,-0.254430867780443,-0.253377355129703,-0.252810094191357,
-0.252249496564011,-0.251559880463779,-0.250822756417118,-0.24964891974005,
-0.235827407491852,-0.204478681377695,-0.192326481256771,-0.179475010979865,
-0.0992817518153433,-0.0941736302836654,-0.0924263964261471,-0.0914365858229751,
-0.0905290460283361,-0.0893088400560055,-0.0880140445847176,-0.0859778652052487,
-0.07142706603922,-0.000961713208880687),.UNSPECIFIED.);
#178=B_SPLINE_CURVE_WITH_KNOTS('',3,(#31177,#31178,#31179,#31180,#31181,
#31182,#31183,#31184,#31185,#31186,#31187,#31188,#31189,#31190,#31191,#31192,
#31193,#31194,#31195,#31196,#31197,#31198,#31199,#31200,#31201,#31202,#31203,
#31204,#31205,#31206,#31207,#31208,#31209,#31210,#31211,#31212,#31213,#31214,
#31215,#31216,#31217,#31218,#31219,#31220,#31221,#31222,#31223,#31224,#31225,
#31226,#31227,#31228,#31229,#31230,#31231,#31232,#31233,#31234,#31235,#31236,
#31237,#31238,#31239,#31240,#31241,#31242,#31243,#31244,#31245,#31246,#31247,
#31248,#31249,#31250,#31251,#31252,#31253,#31254,#31255,#31256,#31257,#31258,
#31259,#31260,#31261,#31262,#31263,#31264,#31265,#31266,#31267,#31268,#31269,
#31270,#31271,#31272,#31273,#31274,#31275,#31276,#31277,#31278,#31279,#31280,
#31281,#31282,#31283,#31284,#31285,#31286,#31287,#31288,#31289,#31290,#31291,
#31292,#31293,#31294,#31295,#31296,#31297,#31298,#31299,#31300,#31301,#31302,
#31303,#31304,#31305,#31306,#31307,#31308,#31309,#31310,#31311,#31312,#31313,
#31314,#31315,#31316,#31317,#31318,#31319,#31320,#31321,#31322,#31323,#31324,
#31325,#31326,#31327,#31328,#31329,#31330,#31331,#31332,#31333,#31334,#31335,
#31336,#31337,#31338,#31339,#31340,#31341,#31342,#31343,#31344,#31345,#31346,
#31347,#31348,#31349,#31350,#31351,#31352,#31353,#31354,#31355,#31356,#31357,
#31358,#31359,#31360,#31361,#31362,#31363,#31364,#31365,#31366,#31367,#31368,
#31369,#31370,#31371,#31372,#31373,#31374,#31375,#31376,#31377,#31378,#31379,
#31380,#31381,#31382,#31383,#31384,#31385,#31386,#31387,#31388),
 .UNSPECIFIED.,.F.,.F.,(4,2,2,2,2,2,2,2,2,2,2,2,2,2,2,2,2,2,2,2,2,2,2,2,
2,2,2,2,2,2,2,2,2,2,2,2,2,2,2,2,2,2,2,2,2,2,2,2,2,2,2,2,2,2,2,2,2,2,2,2,
2,2,2,2,2,2,2,2,2,2,2,2,2,2,2,2,2,2,2,2,2,2,2,2,2,2,2,2,2,2,2,2,2,2,2,2,
2,2,2,2,2,2,2,2,2,4),(-4.05923983194716,-3.99321314324124,-3.99085281993977,
-3.98964595230853,-3.98889513521332,-3.98819576457848,-3.98763479961503,
-3.98699022511209,-3.98589971888069,-3.98198383015804,-3.91710302758606,
-3.90292332503484,-3.8887812530649,-3.84812030474508,-3.83145431077663,
-3.82948587418539,-3.82778430468028,-3.82669501191882,-3.8256756248618,
-3.82434447707302,-3.82153288675943,-3.80048992725936,-3.79796289195734,
-3.78223587827113,-3.74089080667007,-3.70727527801193,-3.67831340478061,
-3.66775859531027,-3.6667032203646,-3.66601595659678,-3.66536214060095,
-3.66485831290565,-3.66428357111583,-3.66319193431783,-3.65938455327526,
-3.59801733697653,-3.54762186422377,-3.51719127705408,-3.50753684356768,
-3.50601831407394,-3.50463660064491,-3.50361273206204,-3.50266250567028,
-3.50136593462497,-3.4988087324421,-3.47793873738283,-3.47491991104323,
-3.42411055110869,-3.37266898708488,-3.35320366501896,-3.34472415821614,
-3.34339487790831,-3.34269908680512,-3.34213838585762,-3.34157519488595,
-3.34054090911407,-3.33722556866146,-3.28481362755085,-3.23536624646431,
-3.20053167210251,-3.18528301493135,-3.18290588191762,-3.18165478509397,
-3.18074401005344,-3.17976952977881,-3.17838210664701,-3.17459926413326,
-3.11368800684472,-3.06057675435992,-3.03568403802857,-3.02218647654392,
-3.02071189329907,-3.01998602306998,-3.01947469495743,-3.01893741088122,
-3.01818364398593,-3.01619904280879,-2.98518561667614,-2.93394584779512,
-2.89348437829834,-2.87171769633277,-2.86203547376924,-2.85993677071331,
-2.85874963993316,-2.8578452007547,-2.8566869183132,-2.8547276713905,-2.84768731741567,
-2.84408045408066,-2.84046395043769,-2.83997337032818,-2.83607936221074,
-2.83488454535907,-2.83338928057516,-2.82876982538296,-2.76338751758028,
-2.7252217569821,-2.70216418592773,-2.69982155907997,-2.69809220985762,
-2.69731608751809,-2.69674498616846,-2.69621261434858,-2.69547731868621,
-2.6936048244233,-2.69161531677502),.UNSPECIFIED.);
#179=B_SPLINE_CURVE_WITH_KNOTS('',3,(#31394,#31395,#31396,#31397,#31398,
#31399,#31400,#31401,#31402,#31403,#31404,#31405,#31406,#31407,#31408,#31409,
#31410,#31411,#31412,#31413,#31414,#31415,#31416,#31417,#31418,#31419,#31420,
#31421,#31422,#31423,#31424,#31425,#31426,#31427,#31428,#31429,#31430,#31431,
#31432,#31433,#31434,#31435,#31436,#31437,#31438,#31439,#31440,#31441,#31442,
#31443,#31444,#31445,#31446,#31447,#31448,#31449,#31450,#31451,#31452,#31453,
#31454,#31455,#31456,#31457,#31458,#31459,#31460,#31461,#31462,#31463,#31464,
#31465,#31466,#31467,#31468,#31469,#31470,#31471,#31472,#31473,#31474,#31475,
#31476,#31477,#31478,#31479,#31480,#31481,#31482,#31483,#31484,#31485,#31486,
#31487,#31488,#31489,#31490,#31491,#31492,#31493,#31494,#31495,#31496,#31497,
#31498,#31499,#31500,#31501,#31502,#31503,#31504,#31505,#31506,#31507,#31508,
#31509,#31510,#31511,#31512,#31513,#31514,#31515,#31516,#31517,#31518,#31519,
#31520,#31521,#31522,#31523,#31524,#31525,#31526,#31527,#31528,#31529,#31530,
#31531,#31532,#31533,#31534,#31535),.UNSPECIFIED.,.F.,.F.,(4,3,3,3,3,3,
3,3,3,3,3,3,3,3,3,3,3,3,3,3,3,3,3,3,3,3,3,3,3,3,3,3,3,3,3,3,3,3,3,3,3,3,
3,3,3,3,3,4),(279.601746169492,279.694968836592,279.788194706647,279.881447740152,
279.974818258919,280.068250010175,280.161852771942,280.237119038469,280.330191982745,
280.423138822382,280.515987193567,280.608767698222,280.701513020379,280.79424798548,
280.886997403821,280.979846044556,281.072746485167,281.165802381252,281.236833693942,
281.329906638218,281.422853477855,281.51570184904,281.608482353695,281.701227675851,
281.793962640953,281.886712059294,281.979560700029,282.07246114064,282.165517036725,
282.236548349415,282.329621293691,282.422568133328,282.515416504513,282.608197009168,
282.700942331324,282.793677296426,282.886426714767,282.979275355502,283.072175796113,
283.165231692198,283.236263004888,283.329324259851,283.422266293444,283.515114136645,
283.60789190088,283.700628731049,283.793365131737,283.838365347136),
 .UNSPECIFIED.);
#180=B_SPLINE_CURVE_WITH_KNOTS('',3,(#31536,#31537,#31538,#31539,#31540,
#31541,#31542,#31543,#31544,#31545,#31546,#31547,#31548,#31549,#31550,#31551,
#31552,#31553,#31554,#31555,#31556,#31557,#31558,#31559,#31560,#31561,#31562,
#31563,#31564,#31565,#31566,#31567,#31568,#31569,#31570,#31571,#31572,#31573,
#31574,#31575,#31576,#31577,#31578,#31579,#31580,#31581,#31582,#31583,#31584,
#31585,#31586,#31587,#31588,#31589,#31590,#31591,#31592,#31593,#31594,#31595,
#31596,#31597,#31598,#31599,#31600,#31601,#31602,#31603,#31604,#31605,#31606,
#31607,#31608,#31609,#31610,#31611,#31612,#31613,#31614,#31615,#31616,#31617,
#31618,#31619,#31620,#31621,#31622,#31623,#31624,#31625,#31626,#31627,#31628,
#31629,#31630,#31631,#31632,#31633,#31634,#31635,#31636,#31637,#31638,#31639,
#31640,#31641),.UNSPECIFIED.,.F.,.F.,(4,2,2,2,2,2,2,2,2,2,2,2,2,2,2,2,2,
2,2,2,2,2,2,2,2,2,2,2,2,2,2,2,2,2,2,2,2,2,2,2,2,2,2,2,2,2,2,2,2,2,2,2,4),
(-4.06014804983483,-3.97627233438681,-3.9540983489275,-3.94499999060754,
-3.94364269485105,-3.94294661142199,-3.94238573801438,-3.94173842067592,
-3.94063665693829,-3.93661534681092,-3.93616197487211,-3.83281327894976,
-3.81563438869693,-3.7954845909032,-3.78493039389705,-3.7827758412725,-3.78179224787277,
-3.78082040480629,-3.77985437709963,-3.77849835854609,-3.77570439382236,
-3.74664651748312,-3.71659417216206,-3.6958895607374,-3.6551563427794,-3.63790786143977,
-3.62229831450554,-3.62077722836758,-3.62004809810623,-3.61953620227033,
-3.61899993004642,-3.61825006656294,-3.61671389026045,-3.60156765415293,
-3.59955044851104,-3.59804814868023,-3.50174633992608,-3.4802367045534,
-3.46854252317124,-3.46392757857399,-3.46056123883827,-3.45913781847436,
-3.45819224174273,-3.45716299063785,-3.45592498330869,-3.45284580079668,
-3.44519475740641,-3.44337966653802,-3.44131925848713,-3.44081022737214,
-3.43874865156816,-3.43711525853886,-3.39927600084928),.UNSPECIFIED.);
#181=B_SPLINE_CURVE_WITH_KNOTS('',3,(#31642,#31643,#31644,#31645,#31646,
#31647,#31648,#31649,#31650,#31651,#31652,#31653,#31654,#31655,#31656,#31657,
#31658,#31659,#31660,#31661,#31662,#31663,#31664,#31665,#31666,#31667,#31668,
#31669,#31670,#31671,#31672,#31673,#31674,#31675,#31676,#31677,#31678,#31679,
#31680,#31681,#31682,#31683,#31684,#31685,#31686,#31687,#31688,#31689,#31690,
#31691,#31692,#31693,#31694,#31695,#31696,#31697,#31698,#31699,#31700,#31701,
#31702,#31703,#31704,#31705,#31706,#31707,#31708,#31709,#31710,#31711,#31712,
#31713,#31714,#31715,#31716,#31717,#31718,#31719,#31720,#31721,#31722,#31723,
#31724,#31725,#31726,#31727,#31728,#31729,#31730,#31731,#31732,#31733,#31734,
#31735,#31736,#31737,#31738,#31739,#31740,#31741,#31742,#31743,#31744,#31745,
#31746,#31747,#31748,#31749,#31750,#31751,#31752,#31753,#31754,#31755,#31756,
#31757,#31758,#31759,#31760,#31761,#31762,#31763,#31764,#31765,#31766,#31767,
#31768,#31769,#31770,#31771,#31772,#31773,#31774,#31775,#31776,#31777,#31778,
#31779,#31780,#31781,#31782,#31783,#31784,#31785,#31786,#31787,#31788,#31789,
#31790,#31791,#31792,#31793,#31794,#31795,#31796,#31797,#31798,#31799,#31800,
#31801,#31802,#31803,#31804,#31805,#31806,#31807,#31808,#31809,#31810,#31811,
#31812,#31813,#31814,#31815,#31816,#31817,#31818,#31819,#31820,#31821,#31822,
#31823,#31824,#31825,#31826,#31827,#31828,#31829,#31830,#31831,#31832,#31833,
#31834,#31835,#31836,#31837,#31838,#31839,#31840,#31841,#31842,#31843,#31844,
#31845,#31846,#31847,#31848,#31849,#31850,#31851,#31852,#31853,#31854,#31855,
#31856,#31857,#31858,#31859,#31860,#31861,#31862,#31863,#31864,#31865,#31866,
#31867,#31868,#31869,#31870,#31871,#31872,#31873,#31874,#31875,#31876,#31877,
#31878,#31879,#31880,#31881,#31882,#31883,#31884,#31885,#31886,#31887,#31888,
#31889,#31890,#31891,#31892,#31893,#31894,#31895,#31896,#31897,#31898,#31899,
#31900,#31901,#31902,#31903,#31904,#31905,#31906,#31907,#31908,#31909,#31910,
#31911,#31912,#31913,#31914,#31915,#31916,#31917,#31918,#31919,#31920,#31921,
#31922,#31923,#31924,#31925,#31926,#31927,#31928,#31929,#31930,#31931,#31932,
#31933,#31934,#31935,#31936,#31937,#31938,#31939,#31940,#31941),
 .UNSPECIFIED.,.F.,.F.,(4,2,2,2,2,2,2,2,2,2,2,2,2,2,2,2,2,2,2,2,2,2,2,2,
2,2,2,2,2,2,2,2,2,2,2,2,2,2,2,2,2,2,2,2,2,2,2,2,2,2,2,2,2,2,2,2,2,2,2,2,
2,2,2,2,2,2,2,2,2,2,2,2,2,2,2,2,2,2,2,2,2,2,2,2,2,2,2,2,2,2,2,2,2,2,2,2,
2,2,2,2,2,2,2,2,2,2,2,2,2,2,2,2,2,2,2,2,2,2,2,2,2,2,2,2,2,2,2,2,2,2,2,2,
2,2,2,2,2,2,2,2,2,2,2,2,2,2,2,2,2,4),(-2.69161531677502,-2.66975863127559,
-2.59833333423941,-2.55681491066562,-2.53986877882376,-2.53739578120855,
-2.53612781025229,-2.53521471375916,-2.53424703289885,-2.53288458415628,
-2.53006404203878,-2.52248328754017,-2.52066917147998,-2.51860651883555,
-2.51815716531915,-2.51615439304126,-2.51343434507484,-2.51223794799365,
-2.5106657409351,-2.42562089209351,-2.40168041140071,-2.3792362626676,-2.37576459583974,
-2.37475705312234,-2.37413265711828,-2.37356817809527,-2.37284785744027,
-2.37133187915587,-2.36135881229659,-2.32584503346877,-2.30313882825556,
-2.25347891510951,-2.22981349995511,-2.21672833737523,-2.21443089930766,
-2.21321004493171,-2.21220553444244,-2.21119130648906,-2.20932161757998,
-2.20327203202333,-2.09964589395868,-2.05415320249531,-2.05231283231797,
-2.05152440393053,-2.05095103653307,-2.0504215369608,-2.04969757376217,
-2.04826494243929,-2.03649646694038,-2.03565884251949,-2.03528199951603,
-2.03187157186493,-2.03104695559205,-2.03082652130756,-2.00952304334794,
-1.93284316004468,-1.91586941545568,-1.91373382956355,-1.91082838371842,
-1.90958705994939,-1.90752321891598,-1.89401576177496,-1.89177232537155,
-1.89043736821384,-1.8894171575682,-1.88832901595168,-1.88663343240954,
-1.88142743795694,-1.85263253770397,-1.80927929752101,-1.7345363823492,
-1.73015126935101,-1.72901305613939,-1.72835724470118,-1.7278023272166,
-1.72711938891572,-1.72582472574377,-1.71824960573342,-1.70249511442728,
-1.67993871492696,-1.57615085386427,-1.56991613140896,-1.56802414454193,
-1.56700539239621,-1.56601074725647,-1.56482546976944,-1.56266088286365,
-1.55998337424128,-1.50875793597317,-1.4118720608639,-1.40707378289095,
-1.40600188921924,-1.40530489663068,-1.40474392006454,-1.40409718779382,
-1.4029691896418,-1.39818971006601,-1.34334308553238,-1.27932994616557,
-1.24894002507576,-1.24611414281008,-1.24475016038786,-1.24378186467486,
-1.2428083750859,-1.24153552447691,-1.23896730548812,-1.2356621084541,-1.20897675642653,
-1.14963715235865,-1.08766149683926,-1.08394766587589,-1.08286617372197,
-1.08229332471083,-1.08178921549943,-1.08113234591145,-1.07995847408672,
-1.07454601559485,-1.06428086581231,-1.03490157010068,-0.94550780530881,
-0.943948685276739,-0.942753773877978,-0.938709018586882,-0.937799471313907,
-0.937400876123338,-0.935338371134719,-0.933526261676283,-0.925947272321559,
-0.923123833474818,-0.921760477235901,-0.920792375958718,-0.91981903454206,
-0.918545998776772,-0.915972521573023,-0.912661283391196,-0.90517509229076,
-0.882869647019001,-0.838102651494489,-0.765143595793327,-0.761039580315633,
-0.759929254039053,-0.759279907608441,-0.758775256131499,-0.758106913623438,
-0.756880398879024,-0.750626525274491,-0.738116346911481,-0.722281313452548,
-0.682051515293471,-0.661851498152186),.UNSPECIFIED.);
#182=B_SPLINE_CURVE_WITH_KNOTS('',3,(#31947,#31948,#31949,#31950,#31951,
#31952,#31953,#31954,#31955,#31956,#31957,#31958,#31959,#31960,#31961,#31962,
#31963,#31964,#31965,#31966,#31967,#31968,#31969,#31970,#31971,#31972,#31973,
#31974,#31975,#31976,#31977,#31978,#31979,#31980,#31981,#31982,#31983,#31984,
#31985,#31986,#31987,#31988,#31989,#31990,#31991,#31992,#31993,#31994,#31995,
#31996,#31997,#31998,#31999,#32000,#32001,#32002,#32003,#32004,#32005,#32006,
#32007,#32008,#32009,#32010,#32011,#32012,#32013,#32014,#32015,#32016,#32017,
#32018,#32019,#32020,#32021,#32022,#32023,#32024,#32025,#32026,#32027,#32028,
#32029,#32030,#32031,#32032,#32033,#32034,#32035,#32036,#32037,#32038,#32039,
#32040,#32041,#32042,#32043,#32044,#32045,#32046,#32047,#32048,#32049,#32050,
#32051,#32052,#32053,#32054,#32055,#32056,#32057,#32058,#32059,#32060,#32061,
#32062,#32063,#32064,#32065,#32066,#32067,#32068,#32069,#32070,#32071,#32072,
#32073,#32074,#32075,#32076,#32077,#32078,#32079,#32080,#32081,#32082,#32083,
#32084,#32085,#32086,#32087,#32088,#32089,#32090,#32091,#32092,#32093,#32094,
#32095,#32096,#32097,#32098,#32099,#32100,#32101,#32102,#32103,#32104,#32105,
#32106,#32107,#32108,#32109,#32110,#32111,#32112,#32113,#32114,#32115,#32116,
#32117,#32118,#32119,#32120,#32121,#32122,#32123,#32124,#32125,#32126,#32127,
#32128,#32129,#32130,#32131,#32132,#32133,#32134,#32135,#32136,#32137,#32138,
#32139,#32140),.UNSPECIFIED.,.F.,.F.,(4,2,2,2,2,2,2,2,2,2,2,2,2,2,2,2,2,
2,2,2,2,2,2,2,2,2,2,2,2,2,2,2,2,2,2,2,2,2,2,2,2,2,2,2,2,2,2,2,2,2,2,2,2,
2,2,2,2,2,2,2,2,2,2,2,2,2,2,2,2,2,2,2,2,2,2,2,2,2,2,2,2,2,2,2,2,2,2,2,2,
2,2,2,2,2,2,2,4),(-1.36962946327728,-1.35522113359464,-1.25363486513697,
-1.24766842856606,-1.24580887865057,-1.24479667881036,-1.24379197755589,
-1.2425924874766,-1.24036948955681,-1.2375990067608,-1.1751740267707,-1.08960099478755,
-1.08490274856675,-1.08383909731689,-1.08314470479165,-1.0826400027721,
-1.08201105269236,-1.08096261244758,-1.07710682614834,-0.988526140506354,
-0.927669658193646,-0.923920123482608,-0.922537717341603,-0.921564494883401,
-0.920587582155144,-0.919325582573995,-0.916805239219223,-0.913577662701302,
-0.906344368579121,-0.884997542159967,-0.839546137460765,-0.766013276509471,
-0.761811049190314,-0.760690882538198,-0.760039285770672,-0.759478777792869,
-0.758788299546242,-0.757457792863099,-0.749052896954004,-0.730084821141988,
-0.68530174884738,-0.629620176574333,-0.623226227537091,-0.621673734057325,
-0.620477933864338,-0.617505887229563,-0.615788161049915,-0.615255073311271,
-0.613196538249033,-0.611362902684152,-0.603546201782025,-0.60059270160666,
-0.59925485857177,-0.598234150893916,-0.597292864485368,-0.595759805561137,
-0.591721518604337,-0.585930415487845,-0.570059610228783,-0.532771897432884,
-0.455568890971052,-0.453357010350174,-0.439769595928774,-0.438134232423592,
-0.43744714152551,-0.436874791326697,-0.436282148395612,-0.435397665123465,
-0.43294883232243,-0.390978849105762,-0.357727230013845,-0.318118385968153,
-0.305786357423783,-0.299791552671234,-0.298237601030414,-0.29700426618635,
-0.295998350722984,-0.280145278367768,-0.277523783189676,-0.276235671924949,
-0.275225199478065,-0.274282311194023,-0.273182904894614,-0.269953670638996,
-0.241541816256804,-0.221902483840598,-0.133180384072646,-0.116938634166373,
-0.115373604620995,-0.114616497005434,-0.11407814379619,-0.113566922577861,
-0.112842994707471,-0.111349115819227,-0.0972260317227201,-0.0703211750184439,
-0.000962450277454619),.UNSPECIFIED.);
#183=B_SPLINE_CURVE_WITH_KNOTS('',3,(#32141,#32142,#32143,#32144,#32145,
#32146,#32147,#32148,#32149,#32150,#32151,#32152,#32153,#32154,#32155,#32156,
#32157,#32158,#32159,#32160,#32161,#32162,#32163,#32164,#32165,#32166,#32167,
#32168,#32169,#32170,#32171,#32172,#32173,#32174,#32175,#32176,#32177,#32178,
#32179,#32180,#32181,#32182,#32183,#32184,#32185,#32186,#32187,#32188,#32189,
#32190,#32191,#32192,#32193,#32194,#32195,#32196,#32197,#32198,#32199,#32200,
#32201,#32202,#32203,#32204,#32205,#32206,#32207,#32208,#32209,#32210),
 .UNSPECIFIED.,.F.,.F.,(4,3,3,3,3,3,3,3,3,3,3,3,3,3,3,3,3,3,3,3,3,3,3,4),
(283.838365347136,283.931130707637,284.024001664162,284.116935236969,284.210011185465,
284.235977660361,284.329050604637,284.421997444274,284.514845815459,284.607626320114,
284.700371642271,284.793106607372,284.885856025713,284.978704666448,285.071605107059,
285.164661003144,285.235692315834,285.329019191919,285.422219967727,285.515319268183,
285.608340093871,285.701312563782,285.794286693993,285.884931476672),
 .UNSPECIFIED.);
#184=B_SPLINE_CURVE_WITH_KNOTS('',3,(#32212,#32213,#32214,#32215,#32216,
#32217,#32218,#32219,#32220,#32221,#32222,#32223,#32224,#32225,#32226,#32227,
#32228,#32229,#32230,#32231,#32232,#32233,#32234,#32235,#32236,#32237,#32238,
#32239,#32240,#32241,#32242,#32243,#32244,#32245,#32246,#32247,#32248,#32249,
#32250,#32251,#32252,#32253,#32254,#32255,#32256,#32257,#32258,#32259,#32260,
#32261,#32262,#32263,#32264,#32265,#32266,#32267,#32268,#32269,#32270,#32271,
#32272,#32273,#32274,#32275,#32276,#32277,#32278,#32279,#32280,#32281,#32282,
#32283,#32284,#32285,#32286,#32287,#32288,#32289,#32290,#32291,#32292,#32293,
#32294,#32295,#32296,#32297,#32298,#32299,#32300,#32301,#32302,#32303,#32304,
#32305,#32306,#32307,#32308,#32309,#32310,#32311,#32312,#32313,#32314,#32315,
#32316,#32317),.UNSPECIFIED.,.F.,.F.,(4,2,2,2,2,2,2,2,2,2,2,2,2,2,2,2,2,
2,2,2,2,2,2,2,2,2,2,2,2,2,2,2,2,2,2,2,2,2,2,2,2,2,2,2,2,2,2,2,2,2,2,2,4),
(-0.661851498152186,-0.62878770815041,-0.622426769083829,-0.620741194311147,
-0.619539344973217,-0.617814864606714,-0.615752489403866,-0.613183040637154,
-0.611331106699762,-0.607346415168121,-0.601044491102584,-0.599144316014681,
-0.598010388134803,-0.597103075690806,-0.596142074964848,-0.594227719906788,
-0.586915283219504,-0.574529656690142,-0.550759053929635,-0.523801621510284,
-0.449614013788087,-0.438864102791653,-0.437468203658721,-0.436753580704446,
-0.436226421530714,-0.435651002090432,-0.43485170074881,-0.432948943699684,
-0.430333817472526,-0.402374404755727,-0.362420115047496,-0.342627331205157,
-0.315287888133803,-0.280345138323659,-0.277161829476354,-0.275872647423816,
-0.274924009529335,-0.273963748096499,-0.272965945018782,-0.270676460027525,
-0.257626943913925,-0.233730766054508,-0.218776160636162,-0.127020883125178,
-0.115914215812652,-0.114368713049002,-0.113631505979336,-0.113064342891623,
-0.11244790457966,-0.111455922433078,-0.108150927225548,-0.0875907243741109,
-0.000962456779688808),.UNSPECIFIED.);
#185=B_SPLINE_CURVE_WITH_KNOTS('',3,(#32318,#32319,#32320,#32321,#32322,
#32323,#32324,#32325,#32326,#32327,#32328,#32329,#32330,#32331,#32332,#32333,
#32334,#32335,#32336,#32337,#32338,#32339,#32340,#32341,#32342,#32343,#32344,
#32345,#32346,#32347,#32348,#32349,#32350,#32351,#32352,#32353,#32354,#32355,
#32356,#32357,#32358,#32359,#32360,#32361,#32362,#32363,#32364,#32365,#32366,
#32367,#32368,#32369,#32370,#32371,#32372,#32373,#32374,#32375,#32376,#32377,
#32378,#32379,#32380,#32381,#32382,#32383,#32384,#32385,#32386,#32387,#32388,
#32389,#32390,#32391,#32392,#32393,#32394,#32395,#32396,#32397,#32398,#32399,
#32400,#32401,#32402,#32403,#32404,#32405,#32406,#32407,#32408,#32409,#32410,
#32411,#32412,#32413,#32414,#32415,#32416,#32417,#32418,#32419,#32420,#32421,
#32422,#32423,#32424,#32425,#32426,#32427,#32428,#32429,#32430,#32431,#32432,
#32433,#32434,#32435,#32436,#32437,#32438,#32439,#32440,#32441,#32442,#32443,
#32444,#32445,#32446,#32447,#32448,#32449,#32450,#32451,#32452,#32453,#32454,
#32455,#32456,#32457,#32458,#32459),.UNSPECIFIED.,.F.,.F.,(4,3,3,3,3,3,
3,3,3,3,3,3,3,3,3,3,3,3,3,3,3,3,3,3,3,3,3,3,3,3,3,3,3,3,3,3,3,3,3,3,3,3,
3,3,3,3,3,4),(285.884931476672,285.977853410009,286.070768379482,286.163700831097,
286.256961744019,286.350056827274,286.44340065503,286.536744482785,286.629817427061,
286.722764266698,286.815612637883,286.908393142538,287.001138464694,287.093873429795,
287.186622848136,287.279471488871,287.372371929483,287.465427825567,287.536459138258,
287.629532082534,287.722478922171,287.815327293356,287.908107798011,288.000853120167,
288.093588085268,288.186337503609,288.279186144344,288.372086584956,288.46514248104,
288.53617379373,288.629246738006,288.722193577643,288.815041948827,288.907822453483,
289.000567775639,289.09330274074,289.186052159081,289.278900799816,289.371801240428,
289.464857136512,289.535888449203,289.628951438742,289.721894824678,289.814743639923,
289.907520539162,290.000256353257,290.092987040943,290.12159641265),
 .UNSPECIFIED.);
#186=B_SPLINE_CURVE_WITH_KNOTS('',3,(#32464,#32465,#32466,#32467,#32468,
#32469,#32470,#32471,#32472,#32473,#32474,#32475,#32476,#32477,#32478,#32479,
#32480,#32481,#32482,#32483,#32484,#32485,#32486,#32487,#32488,#32489,#32490,
#32491,#32492,#32493,#32494,#32495,#32496,#32497,#32498,#32499,#32500,#32501,
#32502,#32503,#32504,#32505,#32506,#32507,#32508,#32509,#32510,#32511,#32512,
#32513,#32514,#32515,#32516,#32517,#32518,#32519,#32520,#32521,#32522,#32523,
#32524,#32525,#32526,#32527,#32528,#32529,#32530,#32531,#32532,#32533,#32534,
#32535,#32536,#32537,#32538,#32539,#32540,#32541,#32542,#32543,#32544,#32545,
#32546,#32547,#32548,#32549,#32550,#32551,#32552,#32553,#32554,#32555,#32556,
#32557,#32558,#32559,#32560,#32561,#32562,#32563,#32564,#32565,#32566,#32567,
#32568,#32569,#32570,#32571,#32572,#32573,#32574,#32575,#32576,#32577,#32578,
#32579,#32580,#32581,#32582,#32583,#32584,#32585,#32586,#32587,#32588,#32589,
#32590,#32591,#32592,#32593,#32594,#32595,#32596,#32597,#32598,#32599,#32600,
#32601,#32602,#32603,#32604,#32605,#32606,#32607,#32608,#32609,#32610,#32611,
#32612,#32613,#32614,#32615,#32616,#32617,#32618,#32619,#32620,#32621,#32622,
#32623,#32624,#32625,#32626,#32627,#32628,#32629,#32630,#32631,#32632,#32633,
#32634,#32635,#32636,#32637,#32638,#32639,#32640,#32641,#32642,#32643,#32644,
#32645,#32646,#32647,#32648,#32649,#32650,#32651,#32652,#32653,#32654,#32655,
#32656,#32657,#32658,#32659,#32660,#32661,#32662,#32663,#32664,#32665,#32666,
#32667,#32668,#32669,#32670,#32671,#32672,#32673,#32674,#32675,#32676,#32677,
#32678,#32679,#32680,#32681,#32682,#32683,#32684,#32685,#32686,#32687,#32688,
#32689,#32690,#32691,#32692,#32693,#32694,#32695,#32696,#32697,#32698,#32699,
#32700,#32701,#32702,#32703,#32704,#32705,#32706,#32707,#32708,#32709,#32710,
#32711,#32712,#32713,#32714,#32715,#32716,#32717,#32718,#32719,#32720,#32721,
#32722,#32723,#32724,#32725,#32726,#32727,#32728,#32729,#32730,#32731,#32732,
#32733),.UNSPECIFIED.,.F.,.F.,(4,2,2,2,2,2,2,2,2,2,2,2,2,2,2,2,2,2,2,2,
2,2,2,2,2,2,2,2,2,2,2,2,2,2,2,2,2,2,2,2,2,2,2,2,2,2,2,2,2,2,2,2,2,2,2,2,
2,2,2,2,2,2,2,2,2,2,2,2,2,2,2,2,2,2,2,2,2,2,2,2,2,2,2,2,2,2,2,2,2,2,2,2,
2,2,2,2,2,2,2,2,2,2,2,2,2,2,2,2,2,2,2,2,2,2,2,2,2,2,2,2,2,2,2,2,2,2,2,2,
2,2,2,2,2,2,4),(-3.39946882069219,-3.3747953566667,-3.35473878549777,-3.34614186934065,
-3.34480797227182,-3.34411119358856,-3.34355041302804,-3.34298774859426,
-3.34195610759352,-3.3386622723819,-3.28658709080641,-3.23587803266845,
-3.20173510423029,-3.18666802497955,-3.1842980535206,-3.18304846389771,
-3.18213787058331,-3.18116271711466,-3.17977288199556,-3.17597452378808,
-3.11402274281264,-3.06052394859133,-3.03288711168279,-3.02339449477033,
-3.02202784596771,-3.02132415256512,-3.0208160599466,-3.02027023431432,
-3.01932234286432,-3.01665078764087,-2.97488612171436,-2.91362283861595,
-2.89087215272044,-2.86460575711339,-2.86176760679706,-2.86042138330595,
-2.85940323974472,-2.85844324436091,-2.85710948258718,-2.85366137163933,
-2.80172560284016,-2.73192628271962,-2.70965694141235,-2.7005461519022,
-2.69919278536021,-2.69849186464927,-2.69793073560402,-2.6972871703058,
-2.69620112212845,-2.69232760340448,-2.62716973622437,-2.54480280835667,
-2.53965842725503,-2.53795695707984,-2.53686768670171,-2.53584829151332,
-2.53451709145403,-2.53170523942729,-2.51065557881264,-2.50816376113553,
-2.50031386415463,-2.41731035761435,-2.3915618927331,-2.38225779637452,
-2.37723467008438,-2.37609122407451,-2.37543601902907,-2.37493210520939,
-2.37435832042518,-2.3732716367524,-2.36950963015601,-2.36756259803964,
-2.36515406638197,-2.36280639565041,-2.32965639713687,-2.30919463607096,
-2.26855783266484,-2.2379033668598,-2.22492058896002,-2.21731889542604,
-2.21537496298488,-2.21423143997401,-2.21322494685541,-2.21197399707917,
-2.21005329921546,-2.20147214024632,-2.08839052542491,-2.07065961317895,
-2.05484016997293,-2.05331518800577,-2.05258518838787,-2.05207305556517,
-2.05153688171486,-2.05078768942265,-2.04925459292882,-2.03421796510482,
-2.03115426980831,-2.00754170660638,-1.90005731595792,-1.89392338325728,
-1.89204341514703,-1.89102707365398,-1.89002264154938,-1.88880500632726,
-1.88652288289963,-1.87375501198413,-1.84895713237321,-1.75920904399099,
-1.73234319425767,-1.73041870666273,-1.72967453892031,-1.72913972393592,
-1.72856988848492,-1.72780203048415,-1.72607684713483,-1.67940192224438,
-1.57688986440158,-1.57079222038806,-1.56891664632421,-1.56790120131222,
-1.56689672630908,-1.56570221603655,-1.56349553890872,-1.56075433596593,
-1.50400877058759,-1.42005597629361,-1.40865561322051,-1.40707877110983,
-1.40634667932272,-1.40578044653949,-1.40516190464683,-1.40415991931988,
-1.40076132207881,-1.37923116980918,-1.36962946327728),.UNSPECIFIED.);
#187=B_SPLINE_CURVE_WITH_KNOTS('',3,(#32735,#32736,#32737,#32738,#32739,
#32740,#32741,#32742,#32743,#32744,#32745,#32746,#32747,#32748,#32749,#32750,
#32751,#32752,#32753,#32754,#32755,#32756,#32757,#32758,#32759,#32760,#32761,
#32762,#32763,#32764,#32765,#32766,#32767,#32768,#32769,#32770,#32771,#32772,
#32773,#32774,#32775,#32776,#32777,#32778,#32779,#32780,#32781,#32782,#32783,
#32784,#32785,#32786,#32787,#32788,#32789,#32790,#32791,#32792,#32793,#32794,
#32795,#32796,#32797,#32798,#32799,#32800,#32801,#32802,#32803,#32804),
 .UNSPECIFIED.,.F.,.F.,(4,3,3,3,3,3,3,3,3,3,3,3,3,3,3,3,3,3,3,3,3,3,3,4),
(290.12159641265,290.214355285923,290.307217500986,290.40013838856,290.493206279757,
290.535603104676,290.628676048952,290.721622888589,290.814471259773,290.907251764429,
290.999997086585,291.092732051686,291.185481470027,291.278330110762,291.371230551374,
291.464286447458,291.535317760149,291.628979765018,291.722512329929,291.815939595004,
291.909279522268,292.002567165507,292.095842588612,292.168116783851),
 .UNSPECIFIED.);
#188=B_SPLINE_CURVE_WITH_KNOTS('',3,(#32805,#32806,#32807,#32808,#32809,
#32810,#32811,#32812,#32813,#32814,#32815,#32816,#32817,#32818,#32819,#32820,
#32821,#32822,#32823,#32824,#32825,#32826,#32827,#32828,#32829,#32830,#32831,
#32832,#32833,#32834,#32835,#32836,#32837,#32838,#32839,#32840,#32841,#32842,
#32843,#32844,#32845,#32846,#32847,#32848,#32849,#32850,#32851,#32852,#32853,
#32854,#32855,#32856,#32857,#32858,#32859,#32860,#32861,#32862,#32863,#32864,
#32865,#32866,#32867,#32868,#32869,#32870,#32871,#32872,#32873,#32874,#32875,
#32876,#32877,#32878,#32879,#32880,#32881,#32882,#32883,#32884,#32885,#32886,
#32887,#32888,#32889,#32890,#32891,#32892,#32893,#32894,#32895,#32896,#32897,
#32898,#32899,#32900,#32901,#32902,#32903,#32904,#32905,#32906,#32907,#32908,
#32909,#32910,#32911,#32912,#32913,#32914,#32915,#32916,#32917,#32918,#32919,
#32920,#32921,#32922,#32923,#32924,#32925,#32926,#32927,#32928,#32929,#32930,
#32931,#32932,#32933,#32934,#32935,#32936,#32937,#32938,#32939,#32940,#32941,
#32942,#32943,#32944,#32945,#32946,#32947,#32948,#32949,#32950,#32951,#32952,
#32953,#32954,#32955,#32956,#32957,#32958,#32959,#32960,#32961,#32962,#32963,
#32964,#32965,#32966,#32967,#32968,#32969,#32970,#32971,#32972,#32973,#32974,
#32975,#32976,#32977,#32978,#32979,#32980,#32981,#32982,#32983,#32984,#32985,
#32986),.UNSPECIFIED.,.F.,.F.,(4,2,2,2,2,2,2,2,2,2,2,2,2,2,2,2,2,2,2,2,
2,2,2,2,2,2,2,2,2,2,2,2,2,2,2,2,2,2,2,2,2,2,2,2,2,2,2,2,2,2,2,2,2,2,2,2,
2,2,2,2,2,2,2,2,2,2,2,2,2,2,2,2,2,2,2,2,2,2,2,2,2,2,2,2,2,2,2,2,2,2,4),
(-4.06049364980017,-3.96866139070536,-3.95255903839914,-3.9444154364705,
-3.94309564450125,-3.94240737724522,-3.94184693705834,-3.94127902782022,
-3.94022201045625,-3.93672030874366,-3.8801640131647,-3.8300373435895,-3.80706276264304,
-3.78527254650186,-3.78268961523789,-3.7816596482364,-3.78071377924466,
-3.77968431546979,-3.77844649048488,-3.77537005049096,-3.74734732799323,
-3.71697821305132,-3.6962998178066,-3.65608093857318,-3.64017852313725,
-3.62766967682958,-3.62141692146495,-3.62019049188046,-3.61952217824578,
-3.61901754096701,-3.61845272181062,-3.61741098928874,-3.61403666025984,
-3.55820241672813,-3.50778814243148,-3.47643070140119,-3.46696621401963,
-3.46101947008403,-3.45924120706139,-3.45814370834501,-3.45713304752249,
-3.4558431340794,-3.45321254196592,-3.43717746574158,-3.43384312679982,
-3.37212957750837,-3.32470932208807,-3.30695277305295,-3.29870183039683,
-3.29737754200379,-3.29668832811293,-3.29612783737283,-3.29547511009567,
-3.29435025374507,-3.29010159809445,-3.21635846200697,-3.17126001971995,
-3.14988942362271,-3.14264901224802,-3.13941886065546,-3.1368961829819,
-3.13563390021424,-3.13465687985068,-3.13368355509557,-3.13230110724487,
-3.12855208993668,-3.06775336834345,-2.9789500764597,-2.97516854144059,
-2.97412713137047,-2.97349966836303,-2.9729356163634,-2.97220814106656,
-2.9706963011772,-2.96082353092394,-2.95829942735653,-2.95727566983203,
-2.95517028747666,-2.95347412150494,-2.87433020000749,-2.81798145144374,
-2.81550027424065,-2.81401931847202,-2.812681603728,-2.81167863470589,-2.81072678607212,
-2.80942503547035,-2.80616880559577,-2.76756834632102,-2.70523002298853,
-2.69196489035576),.UNSPECIFIED.);
#189=B_SPLINE_CURVE_WITH_KNOTS('',3,(#32992,#32993,#32994,#32995,#32996,
#32997,#32998,#32999,#33000,#33001,#33002,#33003,#33004,#33005,#33006,#33007,
#33008,#33009,#33010,#33011,#33012,#33013,#33014,#33015,#33016,#33017,#33018,
#33019,#33020,#33021,#33022,#33023,#33024,#33025,#33026,#33027,#33028,#33029,
#33030,#33031,#33032,#33033,#33034,#33035,#33036,#33037,#33038,#33039,#33040,
#33041,#33042,#33043,#33044,#33045,#33046,#33047,#33048,#33049,#33050,#33051,
#33052,#33053,#33054,#33055,#33056,#33057,#33058,#33059,#33060,#33061,#33062,
#33063,#33064,#33065,#33066,#33067,#33068,#33069,#33070,#33071,#33072,#33073,
#33074,#33075,#33076,#33077,#33078,#33079,#33080,#33081,#33082,#33083,#33084,
#33085,#33086,#33087,#33088,#33089,#33090,#33091,#33092,#33093,#33094,#33095,
#33096,#33097,#33098,#33099,#33100,#33101,#33102,#33103,#33104,#33105,#33106,
#33107,#33108,#33109,#33110,#33111,#33112,#33113,#33114,#33115,#33116,#33117,
#33118,#33119,#33120,#33121,#33122,#33123,#33124,#33125,#33126,#33127,#33128,
#33129,#33130,#33131,#33132,#33133,#33134,#33135,#33136,#33137,#33138,#33139,
#33140,#33141,#33142,#33143,#33144,#33145,#33146,#33147,#33148,#33149,#33150,
#33151,#33152,#33153,#33154,#33155,#33156,#33157,#33158,#33159,#33160,#33161,
#33162,#33163,#33164,#33165,#33166,#33167,#33168,#33169,#33170,#33171,#33172,
#33173,#33174,#33175,#33176,#33177,#33178,#33179,#33180,#33181,#33182,#33183),
 .UNSPECIFIED.,.F.,.F.,(4,2,2,2,2,2,2,2,2,2,2,2,2,2,2,2,2,2,2,2,2,2,2,2,
2,2,2,2,2,2,2,2,2,2,2,2,2,2,2,2,2,2,2,2,2,2,2,2,2,2,2,2,2,2,2,2,2,2,2,2,
2,2,2,2,2,2,2,2,2,2,2,2,2,2,2,2,2,2,2,2,2,2,2,2,2,2,2,2,2,2,2,2,2,2,2,4),
(-1.37001951989838,-1.33384195289187,-1.26133785759749,-1.24760580787192,
-1.23654230157084,-1.22495630350067,-1.22352980407576,-1.22280731905288,
-1.22227812068599,-1.22170429146137,-1.22113582362372,-1.21974712171214,
-1.2095995986987,-1.18308104469748,-1.12352466489329,-1.06710228130897,
-1.0633697212079,-1.06198971529999,-1.06101696096122,-1.06010501517379,
-1.05884796509702,-1.05640955239577,-1.03990757588112,-1.00033093638571,
-0.947195837943482,-0.903720431137309,-0.900932954136615,-0.899968085314147,
-0.899418688458909,-0.898911281841867,-0.898214619850739,-0.896882283209202,
-0.888337738108694,-0.868550043038094,-0.814546528250962,-0.745185651351431,
-0.740673568241149,-0.739013276713724,-0.738040788504815,-0.737128773352301,
-0.735871129118376,-0.734524479869948,-0.728222842193891,-0.718021986793223,
-0.682337936791953,-0.635731134367314,-0.598076770995967,-0.596458298713943,
-0.594800544145728,-0.591809615152871,-0.591283188419006,-0.579081164603803,
-0.577493919732226,-0.576748377870124,-0.576179961505855,-0.575567406708466,
-0.574939023825919,-0.573105369800482,-0.544728635128748,-0.500107086275291,
-0.451910338511425,-0.441517513350794,-0.419885336804425,-0.417014281960592,
-0.41569165656435,-0.414673252016707,-0.413579571932325,-0.411859799344166,
-0.409865506868128,-0.396389610103376,-0.365446471370298,-0.341222376621425,
-0.318160566437614,-0.274517963715436,-0.272105182548319,-0.256372834912897,
-0.254649353402521,-0.253958355429252,-0.253384943163644,-0.252793570499035,
-0.25219671151592,-0.25136007156341,-0.246251348546714,-0.207546439446267,
-0.194651593239625,-0.181213869054641,-0.100239945664783,-0.0950341502386947,
-0.0932732621206296,-0.0922807486901239,-0.0913737775822311,-0.0901588465965395,
-0.0888713470097294,-0.0868524128794112,-0.0723359041243272,-0.000961742289995632),
 .UNSPECIFIED.);
#190=B_SPLINE_CURVE_WITH_KNOTS('',3,(#33184,#33185,#33186,#33187,#33188,
#33189,#33190,#33191,#33192,#33193,#33194,#33195,#33196,#33197,#33198,#33199,
#33200,#33201,#33202,#33203,#33204,#33205,#33206,#33207,#33208,#33209,#33210,
#33211,#33212,#33213,#33214,#33215,#33216,#33217,#33218,#33219,#33220,#33221,
#33222,#33223,#33224,#33225,#33226,#33227,#33228,#33229,#33230,#33231,#33232,
#33233,#33234,#33235,#33236,#33237,#33238,#33239,#33240,#33241,#33242,#33243,
#33244,#33245,#33246,#33247,#33248,#33249,#33250,#33251,#33252,#33253,#33254,
#33255,#33256,#33257,#33258,#33259,#33260,#33261,#33262,#33263,#33264,#33265,
#33266,#33267,#33268,#33269,#33270,#33271,#33272,#33273,#33274,#33275),
 .UNSPECIFIED.,.F.,.F.,(4,2,2,2,2,2,2,2,2,2,2,2,2,2,2,2,2,2,2,2,2,2,2,2,
2,2,2,2,2,2,2,2,2,2,2,2,2,2,2,2,2,2,2,2,2,4),(-4.05995217237598,-3.99475064873395,
-3.99239309084335,-3.99118726501826,-3.99043689203184,-3.98973784624697,
-3.98918206399342,-3.9885391678781,-3.9874557803825,-3.98360629885765,-3.91942180184273,
-3.9051376068729,-3.8908785334912,-3.85007080180934,-3.83336891425697,-3.83124479407454,
-3.82991318853611,-3.82866655327123,-3.82775637303666,-3.82678000793462,
-3.82509844524642,-3.82044281481705,-3.74962028963249,-3.74162419627269,
-3.70879809816409,-3.6798014111963,-3.66924699556814,-3.66818817714662,
-3.6674994680967,-3.66684462282559,-3.66634077235861,-3.66576683106831,
-3.66467917256168,-3.66090773211612,-3.60017045671843,-3.54848408029227,
-3.5148781270311,-3.50849986378626,-3.50714908002633,-3.50588858365521,
-3.50497656199414,-3.50400599795984,-3.50235376785339,-3.49789099074952,
-3.42492520502034,-3.39946882069219),.UNSPECIFIED.);
#191=B_SPLINE_CURVE_WITH_KNOTS('',3,(#33276,#33277,#33278,#33279,#33280,
#33281,#33282,#33283,#33284,#33285,#33286,#33287,#33288,#33289,#33290,#33291,
#33292,#33293,#33294,#33295,#33296,#33297,#33298,#33299,#33300,#33301,#33302,
#33303,#33304,#33305,#33306,#33307,#33308,#33309,#33310,#33311,#33312,#33313,
#33314,#33315,#33316,#33317,#33318,#33319,#33320,#33321,#33322,#33323,#33324,
#33325,#33326,#33327,#33328,#33329,#33330,#33331,#33332,#33333,#33334,#33335,
#33336,#33337,#33338,#33339,#33340,#33341,#33342,#33343,#33344,#33345,#33346,
#33347,#33348,#33349,#33350,#33351,#33352,#33353,#33354,#33355,#33356,#33357,
#33358,#33359,#33360,#33361,#33362,#33363,#33364,#33365,#33366,#33367,#33368,
#33369,#33370,#33371,#33372,#33373,#33374,#33375,#33376,#33377,#33378,#33379,
#33380,#33381,#33382,#33383,#33384,#33385,#33386,#33387,#33388,#33389,#33390,
#33391,#33392,#33393,#33394,#33395,#33396,#33397,#33398,#33399,#33400,#33401,
#33402,#33403,#33404,#33405,#33406,#33407,#33408,#33409,#33410,#33411,#33412,
#33413,#33414,#33415,#33416,#33417,#33418,#33419,#33420,#33421,#33422,#33423,
#33424,#33425,#33426,#33427,#33428,#33429,#33430,#33431,#33432,#33433,#33434,
#33435,#33436,#33437,#33438,#33439,#33440,#33441,#33442,#33443,#33444,#33445,
#33446,#33447,#33448,#33449,#33450,#33451,#33452,#33453,#33454,#33455,#33456,
#33457,#33458,#33459,#33460,#33461,#33462,#33463,#33464,#33465,#33466,#33467,
#33468,#33469,#33470,#33471,#33472,#33473,#33474,#33475,#33476,#33477,#33478,
#33479,#33480,#33481,#33482,#33483,#33484,#33485,#33486,#33487,#33488,#33489,
#33490,#33491,#33492,#33493,#33494,#33495,#33496,#33497,#33498,#33499,#33500,
#33501,#33502,#33503,#33504,#33505,#33506,#33507,#33508,#33509,#33510,#33511,
#33512,#33513,#33514,#33515,#33516,#33517,#33518,#33519,#33520,#33521,#33522,
#33523,#33524,#33525,#33526,#33527,#33528,#33529,#33530,#33531,#33532,#33533,
#33534,#33535,#33536,#33537,#33538,#33539,#33540,#33541,#33542,#33543,#33544,
#33545,#33546,#33547,#33548,#33549,#33550,#33551,#33552,#33553,#33554,#33555,
#33556,#33557,#33558,#33559,#33560,#33561,#33562,#33563,#33564,#33565,#33566,
#33567,#33568,#33569,#33570,#33571,#33572,#33573,#33574,#33575,#33576,#33577,
#33578,#33579,#33580,#33581,#33582,#33583,#33584,#33585,#33586,#33587,#33588,
#33589,#33590,#33591,#33592,#33593,#33594,#33595,#33596,#33597,#33598,#33599,
#33600,#33601,#33602,#33603,#33604,#33605,#33606,#33607,#33608,#33609,#33610,
#33611),.UNSPECIFIED.,.F.,.F.,(4,2,2,2,2,2,2,2,2,2,2,2,2,2,2,2,2,2,2,2,
2,2,2,2,2,2,2,2,2,2,2,2,2,2,2,2,2,2,2,2,2,2,2,2,2,2,2,2,2,2,2,2,2,2,2,2,
2,2,2,2,2,2,2,2,2,2,2,2,2,2,2,2,2,2,2,2,2,2,2,2,2,2,2,2,2,2,2,2,2,2,2,2,
2,2,2,2,2,2,2,2,2,2,2,2,2,2,2,2,2,2,2,2,2,2,2,2,2,2,2,2,2,2,2,2,2,2,2,2,
2,2,2,2,2,2,2,2,2,2,2,2,2,2,2,2,2,2,2,2,2,2,2,2,2,2,2,2,2,2,2,2,2,2,2,2,
2,2,2,4),(-2.69196489035576,-2.67988559045034,-2.66107800437888,-2.65269711684396,
-2.65136739332156,-2.65067700027773,-2.65011639701367,-2.64946450122639,
-2.64834337365824,-2.64413288301269,-2.64349567442083,-2.54578389547178,
-2.49911939113242,-2.49453620938231,-2.49223385904833,-2.49082735431544,
-2.48954459194083,-2.4885507938991,-2.48758281537956,-2.48622000385684,
-2.48339889374229,-2.47581508456675,-2.47400015382847,-2.47193678833891,
-2.47148933910139,-2.47062461443719,-2.46855371434399,-2.46695506995453,
-2.46575129478937,-2.46444065989919,-2.45827356631885,-2.38571838321001,
-2.330258739869,-2.32852033246666,-2.32775002631261,-2.32717974506188,-2.32664554202916,
-2.32590379118526,-2.32399405212404,-2.29804251249304,-2.25171156679459,
-2.2060888523969,-2.18312433676677,-2.16998034497103,-2.16767958228923,
-2.16645779504977,-2.16545295007134,-2.16443875248404,-2.16257018495806,
-2.15653266842959,-2.05405147146666,-2.03059288953971,-2.02795099538641,
-2.02626273152047,-2.02445389510806,-2.02425389814089,-2.02314305604937,
-2.00721064544119,-2.00548133670361,-2.00478934362467,-2.00421563456035,
-2.00362452575462,-2.00274764102565,-2.00035253988194,-1.96210329101591,
-1.85430008258221,-1.85168624365058,-1.84587572233047,-1.84403529750454,
-1.84302680189967,-1.84212202067322,-1.84093412102918,-1.83879026784531,
-1.82850126216438,-1.8090713693667,-1.78519956919261,-1.70098479676786,
-1.69895577251532,-1.68399892624409,-1.68232056654595,-1.68162576425897,
-1.68105134834994,-1.68046125311061,-1.67960676025654,-1.67734877790507,
-1.62938870886335,-1.54844085202926,-1.54539611703954,-1.52454507442936,
-1.52198772160104,-1.52069082578682,-1.51974024311909,-1.51871587810522,
-1.51733329848258,-1.5142925425652,-1.45011390999799,-1.37512112675312,
-1.37479316486045,-1.37387542093885,-1.37341923927877,-1.37263447660971,
-1.36079264237841,-1.35935724985527,-1.3586325032763,-1.35810272307618,
-1.35752934585705,-1.3567572753458,-1.35499762202247,-1.35260484985482,
-1.2710783283939,-1.22588723761503,-1.22162903142905,-1.21934424734738,
-1.21812198170695,-1.21630783992385,-1.21422370822404,-1.21224081883573,
-1.21077579873681,-1.20721482531136,-1.20576588225377,-1.19983229342685,
-1.19797641401661,-1.1969647384673,-1.19595962164296,-1.19473348633175,
-1.19241247272377,-1.18091295522845,-1.15804148871034,-1.08276423329172,
-1.03946705626177,-1.03668747423758,-1.03572378946233,-1.03517462172065,
-1.03466713992901,-1.03396994051874,-1.03263511779166,-1.02402679529242,
-1.0039291879329,-0.948086213892002,-0.902803771305496,-0.898893146005888,
-0.893881055616372,-0.891801761847728,-0.891154082310333,-0.890039029968144,
-0.889115540919865,-0.887289902427046,-0.883327565552538,-0.876973433301037,
-0.875066941199996,-0.873931479739374,-0.873024199062098,-0.871807070094902,
-0.869528576053658,-0.857095394282192,-0.838747158648885,-0.799647291606531,
-0.759559952187023,-0.716546212439798,-0.713780390124337,-0.712818425487851,
-0.712269602632748,-0.711762029549724,-0.71106408384531,-0.709725724526045,
-0.701025637766398,-0.680505225341358,-0.661714306709516),.UNSPECIFIED.);
#192=B_SPLINE_CURVE_WITH_KNOTS('',3,(#33616,#33617,#33618,#33619,#33620,
#33621,#33622,#33623,#33624,#33625,#33626,#33627,#33628,#33629,#33630,#33631,
#33632,#33633,#33634,#33635,#33636,#33637,#33638,#33639,#33640,#33641,#33642,
#33643,#33644,#33645,#33646,#33647,#33648,#33649,#33650,#33651,#33652,#33653,
#33654,#33655,#33656,#33657,#33658,#33659,#33660,#33661,#33662,#33663,#33664,
#33665,#33666,#33667,#33668,#33669,#33670,#33671,#33672,#33673,#33674,#33675,
#33676,#33677,#33678,#33679,#33680,#33681,#33682,#33683,#33684,#33685,#33686,
#33687,#33688,#33689,#33690,#33691,#33692,#33693,#33694,#33695,#33696,#33697,
#33698,#33699,#33700,#33701,#33702,#33703,#33704,#33705,#33706,#33707,#33708,
#33709,#33710,#33711,#33712,#33713,#33714,#33715,#33716,#33717,#33718,#33719,
#33720,#33721,#33722,#33723,#33724,#33725,#33726,#33727,#33728,#33729,#33730,
#33731,#33732,#33733,#33734,#33735,#33736,#33737,#33738,#33739,#33740,#33741,
#33742,#33743,#33744,#33745,#33746,#33747,#33748,#33749,#33750,#33751,#33752,
#33753,#33754,#33755,#33756,#33757,#33758,#33759,#33760,#33761,#33762,#33763,
#33764,#33765,#33766,#33767,#33768,#33769,#33770,#33771,#33772,#33773,#33774,
#33775,#33776,#33777,#33778,#33779,#33780,#33781,#33782,#33783,#33784,#33785,
#33786,#33787,#33788,#33789,#33790,#33791,#33792,#33793,#33794,#33795,#33796,
#33797,#33798,#33799,#33800,#33801,#33802,#33803,#33804,#33805,#33806,#33807,
#33808,#33809,#33810,#33811,#33812,#33813,#33814,#33815,#33816,#33817,#33818,
#33819,#33820,#33821,#33822,#33823,#33824,#33825,#33826,#33827,#33828,#33829,
#33830,#33831,#33832,#33833,#33834,#33835,#33836,#33837,#33838,#33839,#33840,
#33841,#33842,#33843,#33844,#33845,#33846,#33847,#33848,#33849,#33850,#33851,
#33852,#33853,#33854,#33855,#33856,#33857,#33858,#33859,#33860,#33861,#33862,
#33863,#33864,#33865,#33866,#33867,#33868,#33869,#33870,#33871,#33872,#33873,
#33874,#33875,#33876,#33877,#33878,#33879,#33880,#33881,#33882,#33883,#33884,
#33885,#33886,#33887,#33888,#33889,#33890,#33891,#33892,#33893,#33894,#33895,
#33896,#33897,#33898,#33899),.UNSPECIFIED.,.F.,.F.,(4,2,2,2,2,2,2,2,2,2,
2,2,2,2,2,2,2,2,2,2,2,2,2,2,2,2,2,2,2,2,2,2,2,2,2,2,2,2,2,2,2,2,2,2,2,2,
2,2,2,2,2,2,2,2,2,2,2,2,2,2,2,2,2,2,2,2,2,2,2,2,2,2,2,2,2,2,2,2,2,2,2,2,
2,2,2,2,2,2,2,2,2,2,2,2,2,2,2,2,2,2,2,2,2,2,2,2,2,2,2,2,2,2,2,2,2,2,2,2,
2,2,2,2,2,2,2,2,2,2,2,2,2,2,2,2,2,2,2,2,2,2,2,4),(-3.40031960104545,-3.37858596566821,
-3.34204290278943,-3.33168699115945,-3.32531132939754,-3.32346950753675,
-3.32234862735041,-3.32133808197795,-3.32004957550031,-3.31742622783241,
-3.30153740563715,-3.30053095438386,-3.29930128700355,-3.29777364376238,
-3.29180859814735,-3.27479264786146,-3.24283400124832,-3.18866203903901,
-3.17114467939654,-3.16292553074839,-3.16160643778006,-3.16091263948229,
-3.16040562404612,-3.1598549752801,-3.1588836576919,-3.15605099527295,-3.1103052125235,
-3.0407147163238,-3.01591881111591,-3.00321260793306,-3.00101774548281,
-2.99976746258046,-2.99885650826735,-2.99788110490574,-2.99649114271921,
-2.99269384864625,-2.93531761642701,-2.87770281134715,-2.8570719781358,
-2.84562529006256,-2.83977837291701,-2.83857819205993,-2.83802966815972,
-2.8375182721867,-2.83698050159037,-2.83622540727387,-2.83423364764439,
-2.80272497666804,-2.7314140934218,-2.69590094049992,-2.6804715464637,-2.67807963767929,
-2.67682844972011,-2.67591738673668,-2.67494238861362,-2.67355387719879,
-2.66976591455326,-2.60902648728431,-2.52019032074541,-2.51770180162407,
-2.51588590489689,-2.51510374180658,-2.51452848317502,-2.5140010453154,
-2.51328543002819,-2.51188577842982,-2.50103889461304,-2.49942857461786,
-2.40946539578203,-2.35958570957843,-2.35566503077078,-2.35413334851507,
-2.35308040908138,-2.3520506535724,-2.35081186621672,-2.34772983687318,
-2.31951045513813,-2.2259320754401,-2.19733700502889,-2.19468992760766,
-2.19276870695664,-2.19196619409804,-2.19139012144277,-2.19086355734503,
-2.19015145757485,-2.18876553612407,-2.17827833288975,-2.17670156006277,
-2.17451949914548,-2.08502621756368,-2.06546906493039,-2.03936091916682,
-2.03312913572029,-2.03131609339564,-2.03031304396214,-2.02930695571249,
-2.02806555586855,-2.02567222034358,-2.01039884511247,-1.97554064878654,
-1.89815227362373,-1.87167018362919,-1.86975148487277,-1.86900816986545,
-1.86847349605867,-1.86790335156602,-1.86713430534119,-1.86540323608492,
-1.81571242479545,-1.71614175700479,-1.71008966041106,-1.70821930026172,
-1.70720473354506,-1.7061999024436,-1.70497868121193,-1.70272652743159,
-1.69042830226335,-1.6661152553706,-1.58690869782724,-1.55983328964038,
-1.54799534292228,-1.54656009026855,-1.54583538169979,-1.54530561369377,
-1.54473223422214,-1.54396016034049,-1.54220111552757,-1.53980898108709,
-1.45827977638008,-1.41309223717623,-1.40881050178752,-1.40666508229784,
-1.40545411777425,-1.40421398400976,-1.38835107555408,-1.38572890887072,
-1.38444059029022,-1.38343001168435,-1.38230890890245,-1.38046629664485,
-1.37408171694971,-1.37001951989838),.UNSPECIFIED.);
#193=B_SPLINE_CURVE_WITH_KNOTS('',3,(#33901,#33902,#33903,#33904,#33905,
#33906,#33907,#33908,#33909,#33910,#33911,#33912,#33913,#33914,#33915,#33916,
#33917,#33918,#33919,#33920,#33921,#33922,#33923,#33924,#33925,#33926,#33927,
#33928,#33929,#33930,#33931,#33932,#33933,#33934,#33935,#33936,#33937,#33938,
#33939,#33940,#33941,#33942,#33943,#33944,#33945,#33946,#33947,#33948,#33949,
#33950,#33951,#33952,#33953,#33954,#33955,#33956,#33957,#33958,#33959,#33960,
#33961,#33962,#33963,#33964,#33965,#33966,#33967,#33968,#33969,#33970,#33971,
#33972,#33973,#33974,#33975,#33976,#33977,#33978,#33979,#33980,#33981,#33982,
#33983,#33984,#33985,#33986,#33987,#33988,#33989,#33990,#33991,#33992,#33993,
#33994,#33995,#33996,#33997,#33998,#33999,#34000),.UNSPECIFIED.,.F.,.F.,
(4,2,2,2,2,2,2,2,2,2,2,2,2,2,2,2,2,2,2,2,2,2,2,2,2,2,2,2,2,2,2,2,2,2,2,
2,2,2,2,2,2,2,2,2,2,2,2,2,2,4),(-0.661714306709516,-0.635155861013257,-0.583147181177871,
-0.574707142993514,-0.571366622201943,-0.555318144873497,-0.552686488171391,
-0.551396203393642,-0.550385320760791,-0.549265151959854,-0.547426975559338,
-0.541085059986963,-0.505475926761696,-0.497652337254771,-0.450371680231509,
-0.394414259378906,-0.391021287407128,-0.389977145694693,-0.389411757926836,
-0.388907045632092,-0.388239249353062,-0.387532551854712,-0.384671068759998,
-0.380245335982904,-0.366458966434406,-0.340495778906067,-0.317962982724283,
-0.236109005414714,-0.230819846597213,-0.229047464661966,-0.22805257767202,
-0.227145905011295,-0.225935003271963,-0.223685485098539,-0.220909226800922,
-0.202745987705646,-0.161187663257189,-0.146183727652005,-0.138788425803437,
-0.130217995586827,-0.0806258233802182,-0.0689693567103825,-0.0675403915251483,
-0.0668172791246116,-0.0662879198343354,-0.0657142175003553,-0.0651459714985782,
-0.0643831854514484,-0.0631479869242733,-0.000961264455892619),
 .UNSPECIFIED.);
#194=B_SPLINE_CURVE_WITH_KNOTS('',3,(#34001,#34002,#34003,#34004,#34005,
#34006,#34007,#34008,#34009,#34010,#34011,#34012,#34013,#34014,#34015,#34016,
#34017,#34018,#34019,#34020,#34021,#34022,#34023,#34024,#34025,#34026,#34027,
#34028,#34029,#34030,#34031,#34032,#34033,#34034,#34035,#34036,#34037,#34038,
#34039,#34040,#34041,#34042,#34043,#34044,#34045,#34046,#34047,#34048,#34049,
#34050,#34051,#34052,#34053,#34054,#34055,#34056,#34057,#34058,#34059,#34060,
#34061,#34062,#34063,#34064,#34065,#34066,#34067,#34068,#34069,#34070,#34071,
#34072,#34073,#34074,#34075,#34076,#34077,#34078,#34079,#34080,#34081,#34082,
#34083,#34084,#34085,#34086,#34087,#34088,#34089,#34090,#34091,#34092,#34093,
#34094,#34095,#34096,#34097,#34098,#34099,#34100,#34101,#34102,#34103,#34104,
#34105,#34106,#34107,#34108,#34109,#34110,#34111,#34112,#34113,#34114,#34115,
#34116,#34117,#34118,#34119,#34120,#34121,#34122,#34123,#34124,#34125,#34126,
#34127,#34128,#34129,#34130,#34131,#34132,#34133,#34134,#34135,#34136,#34137,
#34138,#34139,#34140,#34141,#34142,#34143,#34144,#34145,#34146,#34147,#34148,
#34149,#34150,#34151,#34152,#34153,#34154,#34155,#34156,#34157,#34158,#34159,
#34160,#34161,#34162,#34163,#34164,#34165,#34166,#34167,#34168,#34169,#34170,
#34171,#34172,#34173,#34174,#34175,#34176,#34177,#34178,#34179,#34180,#34181,
#34182,#34183,#34184,#34185,#34186,#34187,#34188,#34189,#34190,#34191,#34192),
 .UNSPECIFIED.,.F.,.F.,(4,2,2,2,2,2,2,2,2,2,2,2,2,2,2,2,2,2,2,2,2,2,2,2,
2,2,2,2,2,2,2,2,2,2,2,2,2,2,2,2,2,2,2,2,2,2,2,2,2,2,2,2,2,2,2,2,2,2,2,2,
2,2,2,2,2,2,2,2,2,2,2,2,2,2,2,2,2,2,2,2,2,2,2,2,2,2,2,2,2,2,2,2,2,2,2,4),
(-4.06120250444192,-3.99918442014338,-3.97930631026375,-3.97245430131076,
-3.96935382217528,-3.96689338419594,-3.96563804961657,-3.96472638594267,
-3.96375302634548,-3.96237065236763,-3.95862258174264,-3.90197817663135,
-3.87117623880489,-3.85915084194773,-3.84812713630132,-3.81980140646837,
-3.80615166927202,-3.80510122143711,-3.80441592066061,-3.80387424306457,
-3.80331294082442,-3.80275215296733,-3.80173052296751,-3.79851873396886,
-3.74327229041295,-3.71494410090933,-3.6820950081722,-3.65823012307622,
-3.64615291672165,-3.64389356966248,-3.64268062290855,-3.6417738315662,
-3.64078022087196,-3.63901390721368,-3.63376858894774,-3.55236588816066,
-3.51059901844262,-3.48507450573197,-3.48222466351395,-3.48151912684793,
-3.48097104919064,-3.48045987573046,-3.47992145824065,-3.47916408216207,
-3.47715895957184,-3.44457366375936,-3.43584770632301,-3.42618038379795,
-3.37804415611762,-3.33968680552567,-3.32350191370376,-3.32106250917843,
-3.31981148624461,-3.31890034081292,-3.31792506269318,-3.31625071151002,
-3.31164612546338,-3.24124622179403,-3.19662978553869,-3.17022921840333,
-3.16011078401114,-3.15872301741472,-3.15815464487417,-3.15758087265336,
-3.15705160030086,-3.15632882902214,-3.15490121035853,-3.14328347454265,
-3.1406562807068,-3.13821322748276,-3.1346856309721,-3.12962043349618,-3.11148376149684,
-3.04837543566185,-3.01526736944768,-3.00046351012277,-2.99807808490597,
-2.99683832600884,-2.99592858525164,-2.99494830051684,-2.99354091861809,
-2.98963027343245,-2.92607188418165,-2.86227859042434,-2.8399373648659,
-2.83763714710976,-2.83593073722175,-2.83516938076277,-2.83459790074512,
-2.83406537021941,-2.83333014668725,-2.83145934582591,-2.80775271161947,
-2.79712977109084,-2.714856685761,-2.69222113602705),.UNSPECIFIED.);
#195=B_SPLINE_CURVE_WITH_KNOTS('',3,(#34198,#34199,#34200,#34201,#34202,
#34203,#34204,#34205,#34206,#34207,#34208,#34209,#34210,#34211,#34212,#34213,
#34214,#34215,#34216,#34217,#34218,#34219,#34220,#34221,#34222,#34223,#34224,
#34225,#34226,#34227,#34228,#34229,#34230,#34231,#34232,#34233,#34234,#34235,
#34236,#34237,#34238,#34239,#34240,#34241,#34242,#34243,#34244,#34245,#34246,
#34247,#34248,#34249,#34250,#34251,#34252,#34253,#34254,#34255,#34256,#34257,
#34258,#34259,#34260,#34261,#34262,#34263,#34264,#34265,#34266,#34267,#34268,
#34269,#34270,#34271,#34272,#34273,#34274,#34275,#34276,#34277,#34278,#34279,
#34280,#34281,#34282,#34283,#34284,#34285,#34286,#34287,#34288,#34289,#34290,
#34291,#34292,#34293,#34294,#34295,#34296,#34297,#34298,#34299,#34300,#34301,
#34302,#34303,#34304,#34305,#34306,#34307,#34308,#34309,#34310,#34311,#34312,
#34313,#34314,#34315,#34316,#34317,#34318,#34319,#34320,#34321,#34322,#34323,
#34324,#34325,#34326,#34327,#34328,#34329,#34330,#34331,#34332,#34333,#34334,
#34335,#34336,#34337,#34338,#34339,#34340,#34341,#34342,#34343,#34344,#34345,
#34346,#34347,#34348,#34349,#34350,#34351,#34352,#34353,#34354,#34355,#34356,
#34357,#34358,#34359,#34360,#34361,#34362,#34363,#34364,#34365,#34366,#34367,
#34368,#34369,#34370,#34371,#34372,#34373,#34374,#34375,#34376,#34377,#34378,
#34379,#34380,#34381,#34382,#34383,#34384,#34385,#34386,#34387,#34388,#34389,
#34390,#34391,#34392,#34393,#34394,#34395,#34396,#34397,#34398,#34399,#34400,
#34401,#34402,#34403,#34404,#34405,#34406,#34407),.UNSPECIFIED.,.F.,.F.,
(4,2,2,2,2,2,2,2,2,2,2,2,2,2,2,2,2,2,2,2,2,2,2,2,2,2,2,2,2,2,2,2,2,2,2,
2,2,2,2,2,2,2,2,2,2,2,2,2,2,2,2,2,2,2,2,2,2,2,2,2,2,2,2,2,2,2,2,2,2,2,2,
2,2,2,2,2,2,2,2,2,2,2,2,2,2,2,2,2,2,2,2,2,2,2,2,2,2,2,2,2,2,2,2,2,4),(-1.36937854035984,
-1.3634723172623,-1.36174551579247,-1.36105398332151,-1.36048044199618,
-1.3598892754706,-1.35902954674267,-1.35673782810181,-1.30561628549484,
-1.24518139507054,-1.23373512806729,-1.20443443429959,-1.20163398311029,
-1.20027617363742,-1.19930948876856,-1.19839546191318,-1.197123221391,-1.19473789085815,
-1.17963189870071,-1.14506164471568,-1.0819184269639,-1.05671224188495,
-1.0557654430992,-1.05430451933929,-1.05380442215256,-1.05184664337504,
-1.04032362847726,-1.03874188451195,-1.03800878870454,-1.03744232841611,
-1.03682410748946,-1.03584393506711,-1.03264004028301,-1.0275140900212,
-1.01193481096117,-0.978707848292629,-0.93541628780569,-0.882128556336615,
-0.878666290770821,-0.877329857912462,-0.876368888755633,-0.875350586908099,
-0.8740056306571,-0.871167353657731,-0.835381480546332,-0.771769022766303,
-0.726250094588251,-0.725595403448691,-0.717169854782103,-0.715747541190581,
-0.715028194408765,-0.714465095903045,-0.713833010668201,-0.713176561917826,
-0.710921843950462,-0.707655461199289,-0.698524134151089,-0.673564283352825,
-0.633946561607865,-0.560604246141025,-0.556081471880356,-0.554419573164736,
-0.55344678419226,-0.552534899794554,-0.551278081413968,-0.549932564568261,
-0.543645083808342,-0.508881080530274,-0.501253350917058,-0.455119433085655,
-0.396923393145763,-0.393520610808073,-0.392475334735496,-0.391909747875618,
-0.391349007866288,-0.390656599058156,-0.389915581689917,-0.386570632367781,
-0.381152934825141,-0.364119840930446,-0.340063053735909,-0.317930664649403,
-0.238269110764213,-0.233253075657426,-0.231518773744755,-0.230531577436619,
-0.229623544168816,-0.228398350895961,-0.227096625067705,-0.225043965494342,
-0.208355550753423,-0.165744796485386,-0.150885342385304,-0.143597289840791,
-0.135040167623944,-0.0743255391874357,-0.0706175783568126,-0.0695366968133647,
-0.0689639436512813,-0.0684597903981726,-0.067802685786858,-0.0671109274784547,
-0.0660451376037627,-0.0640569238606386,-0.000961349633723722),
 .UNSPECIFIED.);
#196=B_SPLINE_CURVE_WITH_KNOTS('',3,(#34408,#34409,#34410,#34411,#34412,
#34413,#34414,#34415,#34416,#34417,#34418,#34419,#34420,#34421,#34422,#34423,
#34424,#34425,#34426,#34427,#34428,#34429,#34430,#34431,#34432,#34433,#34434,
#34435,#34436,#34437,#34438,#34439,#34440,#34441,#34442,#34443,#34444,#34445,
#34446,#34447,#34448,#34449,#34450,#34451,#34452,#34453,#34454,#34455,#34456,
#34457,#34458,#34459,#34460,#34461,#34462,#34463,#34464,#34465,#34466,#34467,
#34468,#34469,#34470,#34471,#34472,#34473,#34474,#34475,#34476,#34477,#34478,
#34479,#34480,#34481,#34482,#34483,#34484,#34485,#34486,#34487,#34488,#34489,
#34490,#34491,#34492,#34493,#34494,#34495,#34496,#34497,#34498,#34499,#34500,
#34501,#34502,#34503,#34504,#34505,#34506,#34507,#34508,#34509),
 .UNSPECIFIED.,.F.,.F.,(4,2,2,2,2,2,2,2,2,2,2,2,2,2,2,2,2,2,2,2,2,2,2,2,
2,2,2,2,2,2,2,2,2,2,2,2,2,2,2,2,2,2,2,2,2,2,2,2,2,2,4),(-4.06158595367141,
-4.02191754355619,-3.98734963289,-3.97734833853149,-3.97324013374581,-3.97111533590888,
-3.96978330937464,-3.96853628165005,-3.96753917307828,-3.96654182376634,
-3.96475642043572,-3.95936871268148,-3.87622350691803,-3.86391678081209,
-3.85247414675814,-3.82310764940002,-3.80929454365039,-3.80812519526036,
-3.80739000471178,-3.80670181649038,-3.80614140211298,-3.8055734862844,
-3.80451636353468,-3.80101354542866,-3.74444596338195,-3.72113619440367,
-3.69709789171262,-3.66401823454813,-3.65427615660725,-3.64819485858441,
-3.64686248993489,-3.64561519624684,-3.64461800613461,-3.64347468226601,
-3.64153236229673,-3.63693442007136,-3.5572789157746,-3.51424151727211,
-3.48764104228835,-3.48502935485469,-3.48434259350246,-3.48368906778184,
-3.48318504496849,-3.4826096305786,-3.48151537191065,-3.47768666159424,
-3.47525602581653,-3.47259664401322,-3.47181539190525,-3.42656940651116,
-3.40031960104545),.UNSPECIFIED.);
#197=B_SPLINE_CURVE_WITH_KNOTS('',3,(#34510,#34511,#34512,#34513,#34514,
#34515,#34516,#34517,#34518,#34519,#34520,#34521,#34522,#34523,#34524,#34525,
#34526,#34527,#34528,#34529,#34530,#34531,#34532,#34533,#34534,#34535,#34536,
#34537,#34538,#34539,#34540,#34541,#34542,#34543,#34544,#34545,#34546,#34547,
#34548,#34549,#34550,#34551,#34552,#34553,#34554,#34555,#34556,#34557,#34558,
#34559,#34560,#34561,#34562,#34563,#34564,#34565,#34566,#34567,#34568,#34569,
#34570,#34571,#34572,#34573,#34574,#34575,#34576,#34577,#34578,#34579,#34580,
#34581,#34582,#34583,#34584,#34585,#34586,#34587,#34588,#34589,#34590,#34591,
#34592,#34593,#34594,#34595,#34596,#34597,#34598,#34599,#34600,#34601,#34602,
#34603,#34604,#34605,#34606,#34607,#34608,#34609,#34610,#34611,#34612,#34613,
#34614,#34615,#34616,#34617,#34618,#34619,#34620,#34621,#34622,#34623,#34624,
#34625,#34626,#34627,#34628,#34629,#34630,#34631,#34632,#34633,#34634,#34635,
#34636,#34637,#34638,#34639,#34640,#34641,#34642,#34643,#34644,#34645,#34646,
#34647,#34648,#34649,#34650,#34651,#34652,#34653,#34654,#34655,#34656,#34657,
#34658,#34659,#34660,#34661,#34662,#34663,#34664,#34665,#34666,#34667,#34668,
#34669,#34670,#34671,#34672,#34673,#34674,#34675,#34676,#34677,#34678,#34679,
#34680,#34681,#34682,#34683,#34684,#34685,#34686,#34687,#34688,#34689,#34690,
#34691,#34692,#34693,#34694,#34695,#34696,#34697,#34698,#34699,#34700,#34701,
#34702,#34703,#34704,#34705,#34706,#34707,#34708,#34709,#34710,#34711,#34712,
#34713,#34714,#34715,#34716,#34717,#34718,#34719,#34720,#34721,#34722,#34723,
#34724,#34725,#34726,#34727,#34728,#34729,#34730,#34731,#34732,#34733,#34734,
#34735,#34736,#34737,#34738,#34739,#34740,#34741,#34742,#34743,#34744,#34745,
#34746,#34747,#34748,#34749,#34750,#34751,#34752,#34753,#34754,#34755,#34756,
#34757,#34758,#34759,#34760,#34761,#34762,#34763,#34764,#34765,#34766,#34767,
#34768,#34769,#34770,#34771,#34772,#34773,#34774,#34775,#34776,#34777,#34778,
#34779,#34780,#34781,#34782,#34783,#34784,#34785,#34786,#34787,#34788,#34789,
#34790,#34791,#34792,#34793,#34794,#34795,#34796,#34797,#34798,#34799,#34800,
#34801,#34802,#34803,#34804,#34805,#34806,#34807,#34808,#34809,#34810,#34811,
#34812,#34813,#34814,#34815,#34816,#34817,#34818,#34819,#34820,#34821,#34822,
#34823,#34824,#34825,#34826,#34827,#34828,#34829,#34830,#34831,#34832,#34833,
#34834,#34835,#34836,#34837,#34838,#34839,#34840,#34841,#34842,#34843,#34844,
#34845,#34846,#34847,#34848,#34849,#34850,#34851,#34852,#34853,#34854,#34855,
#34856,#34857,#34858,#34859),.UNSPECIFIED.,.F.,.F.,(4,2,2,2,2,2,2,2,2,2,
2,2,2,2,2,2,2,2,2,2,2,2,2,2,2,2,2,2,2,2,2,2,2,2,2,2,2,2,2,2,2,2,2,2,2,2,
2,2,2,2,2,2,2,2,2,2,2,2,2,2,2,2,2,2,2,2,2,2,2,2,2,2,2,2,2,2,2,2,2,2,2,2,
2,2,2,2,2,2,2,2,2,2,2,2,2,2,2,2,2,2,2,2,2,2,2,2,2,2,2,2,2,2,2,2,2,2,2,2,
2,2,2,2,2,2,2,2,2,2,2,2,2,2,2,2,2,2,2,2,2,2,2,2,2,2,2,2,2,2,2,2,2,2,2,2,
2,2,2,2,2,2,2,2,2,2,2,2,2,2,2,2,2,2,2,2,4),(-2.69222113602705,-2.69007669244753,
-2.67728559886547,-2.67498980848289,-2.67376902408037,-2.67276415203694,
-2.67174920237658,-2.66987714919404,-2.66381169811061,-2.66239029506412,
-2.65889458212385,-2.65771365598455,-2.65549007621675,-2.650889079938,-2.64873016428556,
-2.64248768955844,-2.63052833642712,-2.56038567940658,-2.53834384451203,
-2.51684845917666,-2.51459984263146,-2.5129260113745,-2.51216977746626,
-2.51159919277191,-2.51106530616863,-2.51032490437566,-2.50882741850581,
-2.49505223644312,-2.40113804136929,-2.3731638340581,-2.35533559392732,
-2.35244056477934,-2.35104898228777,-2.35002306809675,-2.34907467663945,
-2.34778633313151,-2.34460762651765,-2.30987302819446,-2.24691799208005,
-2.19411403221177,-2.19046574208848,-2.18943758639017,-2.18881310802637,
-2.18824837779029,-2.18752750157517,-2.18600948988397,-2.17600042327404,
-2.10549370050932,-2.06349067728953,-2.04216042947883,-2.03111750406284,
-2.02914656545614,-2.02787976873134,-2.02687153132289,-2.02573774188552,
-2.0238384252863,-2.01673629678524,-1.96837956833978,-1.8791335806374,-1.86832437764547,
-1.8669260711565,-1.86621077209071,-1.86568338541584,-1.86510799565668,
-1.86430922530314,-1.86241001255689,-1.85980111600087,-1.8319672512943,
-1.73464967918419,-1.72845447312895,-1.72709239599361,-1.72588815288837,
-1.72433173773147,-1.72225667399598,-1.7215350553389,-1.72078934587171,
-1.71882216875239,-1.71677840310659,-1.70839492383262,-1.70619283039254,
-1.70486991665283,-1.70385148127936,-1.70275795599506,-1.7010388204461,
-1.69575546139575,-1.66607484520001,-1.62177233162103,-1.56215191164498,
-1.5597680068299,-1.55860096947444,-1.55768257961346,-1.55583963904399,
-1.54525402936251,-1.54386436858947,-1.54315133126318,-1.5426245548735,
-1.54204874431662,-1.54124747040194,-1.53937190952313,-1.53678396528969,
-1.50935321250065,-1.43086455788118,-1.41287338972399,-1.40600106481876,
-1.40450612811347,-1.40331105485673,-1.39929948212293,-1.39856349846819,
-1.39786461242248,-1.39586020692061,-1.39363462371044,-1.38493149462545,
-1.38300040248388,-1.38174599027947,-1.38073889935247,-1.3795970567498,
-1.37770039473882,-1.37057596613914,-1.32162842904402,-1.25626955417356,
-1.2433875971673,-1.2416231741618,-1.2375937216333,-1.23683685254952,-1.2360231631778,
-1.22245729530725,-1.22082246530989,-1.22013541172246,-1.21956301247527,
-1.21897023129467,-1.2181031751475,-1.21575644509737,-1.1588175552152,-1.10529876343665,
-1.08818156626407,-1.08246838123858,-1.08106716718255,-1.07985348307207,
-1.07868891529225,-1.06278993416567,-1.06016589474539,-1.05887717959003,
-1.05786653079516,-1.05674559778234,-1.05494064439751,-1.04876535413208,
-1.02273995520031,-0.983768457662749,-0.939087701672631,-0.908653661530226,
-0.907330552650375,-0.905778085018777,-0.903340941370666,-0.902040061870972,
-0.898559695140791,-0.89750512534783,-0.896937665081658,-0.896377109344793,
-0.895687891046809,-0.894390377903307,-0.887647876153156,-0.873572102083395,
-0.854749327332244,-0.807608709245875,-0.793046201470491,-0.741237434638338,
-0.737789388646109,-0.736455278726315,-0.735494905655486,-0.734476244411601,
-0.733129139751278,-0.730236829094953,-0.705472169583721,-0.684076569345851,
-0.662296405813887),.UNSPECIFIED.);
#198=B_SPLINE_CURVE_WITH_KNOTS('',3,(#34864,#34865,#34866,#34867,#34868,
#34869,#34870,#34871,#34872,#34873,#34874,#34875,#34876,#34877,#34878,#34879,
#34880,#34881,#34882,#34883,#34884,#34885,#34886,#34887,#34888,#34889,#34890,
#34891,#34892,#34893,#34894,#34895,#34896,#34897,#34898,#34899,#34900,#34901,
#34902,#34903,#34904,#34905,#34906,#34907,#34908,#34909,#34910,#34911,#34912,
#34913,#34914,#34915,#34916,#34917,#34918,#34919,#34920,#34921,#34922,#34923,
#34924,#34925,#34926,#34927,#34928,#34929,#34930,#34931,#34932,#34933,#34934,
#34935,#34936,#34937,#34938,#34939,#34940,#34941,#34942,#34943,#34944,#34945,
#34946,#34947,#34948,#34949,#34950,#34951,#34952,#34953,#34954,#34955,#34956,
#34957,#34958,#34959,#34960,#34961,#34962,#34963,#34964,#34965,#34966,#34967,
#34968,#34969,#34970,#34971,#34972,#34973,#34974,#34975,#34976,#34977,#34978,
#34979,#34980,#34981,#34982,#34983,#34984,#34985,#34986,#34987,#34988,#34989,
#34990,#34991,#34992,#34993,#34994,#34995,#34996,#34997,#34998,#34999,#35000,
#35001,#35002,#35003,#35004,#35005,#35006,#35007,#35008,#35009,#35010,#35011,
#35012,#35013,#35014,#35015,#35016,#35017,#35018,#35019,#35020,#35021,#35022,
#35023,#35024,#35025,#35026,#35027,#35028,#35029,#35030,#35031,#35032,#35033,
#35034,#35035,#35036,#35037,#35038,#35039,#35040,#35041,#35042,#35043,#35044,
#35045,#35046,#35047,#35048,#35049,#35050,#35051,#35052,#35053,#35054,#35055,
#35056,#35057,#35058,#35059,#35060,#35061,#35062,#35063,#35064,#35065,#35066,
#35067,#35068,#35069,#35070,#35071,#35072,#35073,#35074,#35075,#35076,#35077,
#35078,#35079,#35080,#35081,#35082,#35083,#35084,#35085,#35086,#35087,#35088,
#35089,#35090,#35091,#35092,#35093,#35094,#35095,#35096,#35097,#35098,#35099,
#35100,#35101,#35102,#35103,#35104,#35105,#35106,#35107,#35108,#35109,#35110,
#35111,#35112,#35113,#35114,#35115,#35116,#35117,#35118,#35119,#35120,#35121,
#35122,#35123,#35124,#35125,#35126,#35127,#35128,#35129,#35130,#35131,#35132,
#35133,#35134,#35135,#35136,#35137,#35138,#35139,#35140,#35141,#35142,#35143,
#35144,#35145,#35146,#35147),.UNSPECIFIED.,.F.,.F.,(4,2,2,2,2,2,2,2,2,2,
2,2,2,2,2,2,2,2,2,2,2,2,2,2,2,2,2,2,2,2,2,2,2,2,2,2,2,2,2,2,2,2,2,2,2,2,
2,2,2,2,2,2,2,2,2,2,2,2,2,2,2,2,2,2,2,2,2,2,2,2,2,2,2,2,2,2,2,2,2,2,2,2,
2,2,2,2,2,2,2,2,2,2,2,2,2,2,2,2,2,2,2,2,2,2,2,2,2,2,2,2,2,2,2,2,2,2,2,2,
2,2,2,2,2,2,2,2,2,2,2,2,2,2,2,2,2,2,2,2,2,2,2,4),(-3.3997268905259,-3.3771628241713,
-3.33580946997168,-3.31958623260249,-3.30721025344548,-3.30100650200268,
-3.29978307411547,-3.29911548440289,-3.29861097737682,-3.29796123109853,
-3.29684884046162,-3.29272312729606,-3.21960477459023,-3.17514639748534,
-3.15281336210418,-3.14531925430101,-3.14200545004725,-3.13942995834573,
-3.13815685352547,-3.13718376212722,-3.13621593929206,-3.13485326258567,
-3.13203215755142,-3.12445058329786,-3.1226365225275,-3.12057358681922,
-3.12016219008537,-3.02643096784493,-3.00147711862295,-2.98091306671218,
-2.97760848151872,-2.97661677638162,-2.97600054632386,-2.97543360023269,
-2.97469671107584,-2.97309443211346,-2.96103256157469,-2.96041460730051,
-2.90278757345259,-2.84734695571871,-2.82211988874398,-2.8189222905335,
-2.81642226208569,-2.81516366249859,-2.81418542200147,-2.81321034088773,
-2.81182128215009,-2.80802918953171,-2.74673967723941,-2.70500090975098,
-2.68043397428133,-2.6596548145686,-2.65497819761206,-2.65385833165813,
-2.65321344878749,-2.65265235570614,-2.65195300785722,-2.65087341933944,
-2.64597870660815,-2.55003072503517,-2.52592121695208,-2.50193101117893,
-2.49728351518924,-2.49495755909327,-2.49354127869805,-2.49225164299211,
-2.49125621706937,-2.49029082036903,-2.48866550531583,-2.48437628302639,
-2.41860089249946,-2.3351499001201,-2.331698558582,-2.33069092234302,-2.33007111207734,
-2.3295052518304,-2.32877572167103,-2.32757182070025,-2.32304513326697,
-2.23259528749899,-2.19503804272193,-2.18588006768357,-2.17254437291696,
-2.17023488450645,-2.16901138462147,-2.16800664329261,-2.16699383285271,
-2.16513152212243,-2.15914335936802,-2.04353702228946,-2.03059217753551,
-2.02822635649256,-2.02430165344751,-2.02270650350391,-2.02196214656499,
-2.02066448263749,-2.00945136146132,-2.00788182360996,-2.00715103746717,
-2.00658490884384,-2.00596553805334,-2.00496019221423,-2.00153144610128,
-1.9796886182026,-1.9553774471919,-1.85436570928257,-1.8484384417654,-1.84658350234068,
-1.84557210638145,-1.84456711939132,-1.84334092750096,-1.84101915907977,
-1.82742228024506,-1.80313863628736,-1.71200382155643,-1.70391750093161,
-1.70151150895958,-1.69950436041351,-1.69889340012299,-1.69790082271575,
-1.68632120065326,-1.68489497096213,-1.68417257078319,-1.68364340965114,
-1.68306959561662,-1.68229509191869,-1.68052238064887,-1.67810713535117,
-1.62533341962038,-1.53500396945807,-1.52739156885379,-1.5245908151617,
-1.52323296988438,-1.52226630990573,-1.52135234762095,-1.52008026238806,
-1.51758886072771,-1.50045628761802,-1.45807328684913,-1.38463743457022,
-1.37932198100892,-1.36937854035984),.UNSPECIFIED.);
#199=B_SPLINE_CURVE_WITH_KNOTS('',3,(#35149,#35150,#35151,#35152,#35153,
#35154,#35155,#35156,#35157,#35158,#35159,#35160,#35161,#35162,#35163,#35164,
#35165,#35166,#35167,#35168,#35169,#35170,#35171,#35172,#35173,#35174,#35175,
#35176,#35177,#35178,#35179,#35180,#35181,#35182,#35183,#35184,#35185,#35186,
#35187,#35188,#35189,#35190,#35191,#35192,#35193,#35194,#35195,#35196,#35197,
#35198,#35199,#35200,#35201,#35202,#35203,#35204,#35205,#35206,#35207,#35208,
#35209,#35210,#35211,#35212,#35213,#35214,#35215,#35216,#35217,#35218,#35219,
#35220,#35221,#35222,#35223,#35224,#35225,#35226,#35227,#35228,#35229,#35230,
#35231,#35232,#35233,#35234,#35235,#35236,#35237,#35238,#35239,#35240,#35241,
#35242,#35243,#35244,#35245,#35246,#35247,#35248,#35249,#35250),
 .UNSPECIFIED.,.F.,.F.,(4,2,2,2,2,2,2,2,2,2,2,2,2,2,2,2,2,2,2,2,2,2,2,2,
2,2,2,2,2,2,2,2,2,2,2,2,2,2,2,2,2,2,2,2,2,2,2,2,2,2,4),(-0.662296405813887,
-0.635922143580946,-0.579178057163701,-0.575662803806911,-0.574604087012972,
-0.574035778638131,-0.573475275280843,-0.57278740858407,-0.572052717946922,
-0.568798381618287,-0.541102743316805,-0.495436529670279,-0.46387662861801,
-0.418219735819375,-0.414848173644762,-0.41352676323732,-0.412569725041022,
-0.411549196059965,-0.410190404548335,-0.408703849802014,-0.399799199677671,
-0.383732072701302,-0.347123216534896,-0.318961393345521,-0.272701284958046,
-0.271074414713863,-0.268857910349997,-0.267732393027013,-0.266277394276951,
-0.265427885007478,-0.253669165452721,-0.252236632201744,-0.251512608435462,
-0.250983010956051,-0.250409483142604,-0.249620739522225,-0.248745631022214,
-0.24268866252878,-0.203539279748206,-0.190232426429279,-0.17643499218325,
-0.0973312252954645,-0.092457088152077,-0.0907347286850655,-0.0897498971626706,
-0.0888412984790158,-0.0876112148140803,-0.0863027256173666,-0.084234053599299,
-0.0696288491241501,-0.00096165502097932),.UNSPECIFIED.);
#200=B_SPLINE_CURVE_WITH_KNOTS('',3,(#35251,#35252,#35253,#35254,#35255,
#35256,#35257,#35258,#35259,#35260,#35261,#35262,#35263,#35264,#35265,#35266,
#35267,#35268,#35269,#35270,#35271,#35272,#35273,#35274,#35275,#35276,#35277,
#35278,#35279,#35280,#35281,#35282,#35283,#35284,#35285,#35286,#35287,#35288,
#35289,#35290,#35291,#35292,#35293,#35294,#35295,#35296,#35297,#35298,#35299,
#35300,#35301,#35302,#35303,#35304,#35305,#35306,#35307,#35308,#35309,#35310,
#35311,#35312,#35313,#35314,#35315,#35316,#35317,#35318,#35319,#35320,#35321,
#35322,#35323,#35324,#35325,#35326,#35327,#35328,#35329,#35330,#35331,#35332,
#35333,#35334,#35335,#35336,#35337,#35338,#35339,#35340,#35341,#35342,#35343,
#35344,#35345,#35346,#35347,#35348,#35349,#35350,#35351,#35352,#35353,#35354,
#35355,#35356,#35357,#35358,#35359,#35360,#35361,#35362,#35363,#35364,#35365,
#35366,#35367,#35368,#35369,#35370,#35371,#35372,#35373,#35374,#35375,#35376,
#35377,#35378,#35379,#35380,#35381,#35382,#35383,#35384,#35385,#35386,#35387,
#35388,#35389,#35390,#35391,#35392),.UNSPECIFIED.,.F.,.F.,(4,3,3,3,3,3,
3,3,3,3,3,3,3,3,3,3,3,3,3,3,3,3,3,3,3,3,3,3,3,3,3,3,3,3,3,3,3,3,3,3,3,3,
3,3,3,3,3,4),(317.30085801257,317.426612624734,317.527898802443,317.620971746719,
317.713918586356,317.806766957541,317.899547462196,317.992292784352,318.085027749454,
318.177777167795,318.27062580853,318.363526249141,318.456582145226,318.527613457915,
318.620686402191,318.713633241828,318.806481613012,318.899262117668,318.992007439824,
319.084742404925,319.177491823266,319.270340464001,319.363240904613,319.456296800697,
319.527328113388,319.620401057664,319.713347897301,319.806196268486,319.898976773141,
319.991722095298,320.084457060399,320.17720647874,320.270055119475,320.362955560087,
320.456011456171,320.527042768861,320.620115713137,320.713062552774,320.805910923959,
320.898691428614,320.99143675077,321.084171715871,321.176921134213,321.269769774948,
321.362670215559,321.455726111644,321.526757424334,321.537850218284),
 .UNSPECIFIED.);
#201=B_SPLINE_CURVE_WITH_KNOTS('',3,(#35398,#35399,#35400,#35401,#35402,
#35403,#35404,#35405,#35406,#35407,#35408,#35409,#35410,#35411,#35412,#35413,
#35414,#35415,#35416,#35417,#35418,#35419,#35420,#35421,#35422,#35423,#35424,
#35425,#35426,#35427,#35428,#35429,#35430,#35431,#35432,#35433,#35434,#35435,
#35436,#35437,#35438,#35439,#35440,#35441,#35442,#35443,#35444,#35445,#35446,
#35447,#35448,#35449,#35450,#35451,#35452,#35453,#35454,#35455,#35456,#35457,
#35458,#35459,#35460,#35461,#35462,#35463,#35464,#35465,#35466,#35467,#35468,
#35469,#35470,#35471,#35472,#35473,#35474,#35475,#35476,#35477,#35478,#35479,
#35480,#35481,#35482,#35483,#35484,#35485,#35486,#35487,#35488,#35489,#35490,
#35491,#35492,#35493,#35494,#35495,#35496,#35497,#35498,#35499,#35500,#35501,
#35502,#35503,#35504,#35505,#35506,#35507,#35508,#35509,#35510,#35511,#35512,
#35513,#35514,#35515,#35516,#35517,#35518,#35519,#35520,#35521,#35522,#35523,
#35524,#35525,#35526,#35527,#35528,#35529,#35530,#35531,#35532,#35533,#35534,
#35535,#35536,#35537,#35538,#35539),.UNSPECIFIED.,.F.,.F.,(4,3,3,3,3,3,
3,3,3,3,3,3,3,3,3,3,3,3,3,3,3,3,3,3,3,3,3,3,3,3,3,3,3,3,3,3,3,3,3,3,3,3,
3,3,3,3,3,4),(323.584043319749,323.677168290332,323.770293186491,323.863442132054,
323.956705811341,324.050028268095,324.143522381568,324.224563879274,324.31763682355,
324.410583663187,324.503432034372,324.596212539027,324.688957861183,324.781692826285,
324.874442244626,324.967290885361,325.060191325973,325.153247222057,325.224278534747,
325.317351479023,325.41029831866,325.503146689845,325.5959271945,325.688672516656,
325.781407481758,325.874156900099,325.967005540834,326.059905981446,326.15296187753,
326.22399319022,326.317066134496,326.410012974133,326.502861345318,326.595641849973,
326.688387172129,326.781122137231,326.873871555572,326.966720196307,327.059620636918,
327.152676533003,327.223707845693,327.316769638063,327.409712089381,327.502560231227,
327.595337701616,327.688074190646,327.780808710477,327.820676619569),
 .UNSPECIFIED.);
#202=B_SPLINE_CURVE_WITH_KNOTS('',3,(#35540,#35541,#35542,#35543,#35544,
#35545,#35546,#35547,#35548,#35549,#35550,#35551,#35552,#35553,#35554,#35555,
#35556,#35557,#35558,#35559,#35560,#35561,#35562,#35563,#35564,#35565,#35566,
#35567,#35568,#35569,#35570,#35571,#35572,#35573,#35574,#35575,#35576,#35577,
#35578,#35579,#35580,#35581,#35582,#35583,#35584,#35585,#35586,#35587,#35588,
#35589,#35590,#35591,#35592,#35593,#35594,#35595,#35596,#35597,#35598,#35599,
#35600,#35601,#35602,#35603,#35604,#35605,#35606,#35607,#35608,#35609,#35610,
#35611,#35612,#35613,#35614,#35615,#35616,#35617,#35618,#35619,#35620,#35621,
#35622,#35623,#35624,#35625,#35626,#35627,#35628,#35629,#35630,#35631,#35632,
#35633),.UNSPECIFIED.,.F.,.F.,(4,2,2,2,2,2,2,2,2,2,2,2,2,2,2,2,2,2,2,2,
2,2,2,2,2,2,2,2,2,2,2,2,2,2,2,2,2,2,2,2,2,2,2,2,2,2,4),(-4.06047020503067,
-3.97913746508193,-3.95675138905933,-3.94703589900244,-3.94565686751046,
-3.94495626897608,-3.9444001811875,-3.94375797944412,-3.94267814510715,
-3.93886372511926,-3.93813114133112,-3.83525091816359,-3.81695395295451,
-3.79727610185871,-3.7869093526443,-3.78476606409044,-3.78378358585031,
-3.78281048023268,-3.78184265310799,-3.78048004407804,-3.77765931877126,
-3.747476617408,-3.71973348977647,-3.70078227916256,-3.6653111829581,-3.63837956341343,
-3.62425204445573,-3.62275850928821,-3.62203480495442,-3.621523763611,-3.62098562019866,
-3.62022884041364,-3.61822646690423,-3.58582521688203,-3.53072754904893,
-3.50179936755701,-3.47731315129606,-3.4688157931356,-3.46517712633776,
-3.4624011630548,-3.46108603969737,-3.46012434331055,-3.45917331974369,
-3.45787408608017,-3.45530690057294,-3.43416462328477,-3.3997268905259),
 .UNSPECIFIED.);
#203=B_SPLINE_CURVE_WITH_KNOTS('',3,(#35635,#35636,#35637,#35638,#35639,
#35640,#35641,#35642,#35643,#35644,#35645,#35646,#35647,#35648,#35649,#35650,
#35651,#35652,#35653,#35654,#35655,#35656,#35657,#35658,#35659,#35660,#35661,
#35662,#35663,#35664,#35665,#35666,#35667,#35668,#35669,#35670,#35671,#35672,
#35673,#35674,#35675,#35676,#35677,#35678,#35679,#35680,#35681,#35682,#35683,
#35684,#35685,#35686,#35687,#35688,#35689,#35690,#35691,#35692,#35693,#35694,
#35695,#35696,#35697,#35698,#35699,#35700,#35701,#35702,#35703,#35704),
 .UNSPECIFIED.,.F.,.F.,(4,3,3,3,3,3,3,3,3,3,3,3,3,3,3,3,3,3,3,3,3,3,3,4),
(321.537850218284,321.630906689133,321.723840353486,321.816678833244,321.909453844202,
322.002196630937,322.094932016044,322.187684809342,322.280538445769,322.373446537988,
322.466506761149,322.526472079807,322.619545024083,322.71249186372,322.805340234905,
322.89812073956,322.990866061716,323.083601026818,323.176350445159,323.269199085894,
323.362099526505,323.45515542259,323.52618673528,323.584043319749),
 .UNSPECIFIED.);
#204=B_SPLINE_CURVE_WITH_KNOTS('',3,(#35705,#35706,#35707,#35708,#35709,
#35710,#35711,#35712,#35713,#35714,#35715,#35716,#35717,#35718,#35719,#35720,
#35721,#35722,#35723,#35724,#35725,#35726,#35727,#35728,#35729,#35730,#35731,
#35732,#35733,#35734,#35735,#35736,#35737,#35738,#35739,#35740,#35741,#35742,
#35743,#35744,#35745,#35746,#35747,#35748,#35749,#35750,#35751,#35752,#35753,
#35754,#35755,#35756,#35757,#35758,#35759,#35760,#35761,#35762,#35763,#35764,
#35765,#35766,#35767,#35768,#35769,#35770,#35771,#35772,#35773,#35774,#35775,
#35776,#35777,#35778,#35779,#35780,#35781,#35782,#35783,#35784,#35785,#35786,
#35787,#35788,#35789,#35790,#35791,#35792,#35793,#35794,#35795,#35796,#35797,
#35798,#35799,#35800,#35801,#35802,#35803,#35804,#35805,#35806,#35807,#35808,
#35809,#35810,#35811,#35812,#35813,#35814,#35815,#35816,#35817,#35818,#35819,
#35820,#35821,#35822,#35823,#35824,#35825,#35826,#35827,#35828,#35829,#35830,
#35831,#35832,#35833,#35834,#35835,#35836,#35837,#35838,#35839,#35840,#35841,
#35842,#35843,#35844,#35845,#35846,#35847,#35848,#35849,#35850,#35851,#35852,
#35853,#35854,#35855,#35856,#35857,#35858,#35859,#35860,#35861,#35862,#35863,
#35864,#35865,#35866,#35867,#35868,#35869,#35870,#35871,#35872,#35873,#35874,
#35875,#35876,#35877,#35878,#35879,#35880,#35881,#35882),.UNSPECIFIED.,
 .F.,.F.,(4,2,2,2,2,2,2,2,2,2,2,2,2,2,2,2,2,2,2,2,2,2,2,2,2,2,2,2,2,2,2,
2,2,2,2,2,2,2,2,2,2,2,2,2,2,2,2,2,2,2,2,2,2,2,2,2,2,2,2,2,2,2,2,2,2,2,2,
2,2,2,2,2,2,2,2,2,2,2,2,2,2,2,2,2,2,2,2,2,4),(-4.06158467854896,-3.94923519837409,
-3.93599991200773,-3.92269161835556,-3.9203844843538,-3.91916195013851,
-3.91815785603613,-3.9171455743914,-3.91528387952344,-3.90929489692491,
-3.80707759085534,-3.780429788445,-3.76619296282042,-3.7616572197697,-3.75970599817688,
-3.75821443572828,-3.75749334496842,-3.75695237577373,-3.75641286978667,
-3.75549628555695,-3.75303613713578,-3.71082729871476,-3.68711829481489,
-3.63534543560341,-3.61305531884369,-3.59988583634365,-3.59758498231347,
-3.59636366562971,-3.59535947704117,-3.59434617080706,-3.59247990733709,
-3.58645506848342,-3.47028488122393,-3.44954831734609,-3.44091754313171,
-3.4377838867191,-3.43629841022243,-3.43543242139521,-3.43465982706144,
-3.43409669173043,-3.43356913708102,-3.43285237877034,-3.43144757090977,
-3.42044944837904,-3.37112334511462,-3.32644618364195,-3.29656769246454,
-3.27729574258921,-3.27476779063671,-3.27349887996492,-3.27258563400271,
-3.27161828333527,-3.27025709911317,-3.26744177157477,-3.23747617525587,
-3.15003519508914,-3.13680805481928,-3.12112328809136,-3.11616714365453,
-3.11408372764611,-3.11298141375338,-3.1122743967749,-3.1116395375029,-3.11109029036474,
-3.11052212319802,-3.10946342741072,-3.10594625200448,-3.10470127127753,
-3.00344560168929,-2.96917199121828,-2.95405383427677,-2.95166753945285,
-2.95042797212063,-2.94943171380618,-2.94843090627298,-2.94662747018178,
-2.94110146240276,-2.82165350108662,-2.79149660831535,-2.79012149833543,
-2.78930070309898,-2.78856044039257,-2.78800292280664,-2.78746653242957,
-2.78671645940916,-2.78475579041022,-2.75550863959052,-2.70226679468588,
-2.69256774355998),.UNSPECIFIED.);
#205=B_SPLINE_CURVE_WITH_KNOTS('',3,(#35888,#35889,#35890,#35891,#35892,
#35893,#35894,#35895,#35896,#35897,#35898,#35899,#35900,#35901,#35902,#35903,
#35904,#35905,#35906,#35907,#35908,#35909,#35910,#35911,#35912,#35913,#35914,
#35915,#35916,#35917,#35918,#35919,#35920,#35921,#35922,#35923,#35924,#35925,
#35926,#35927,#35928,#35929,#35930,#35931,#35932,#35933,#35934,#35935,#35936,
#35937,#35938,#35939,#35940,#35941,#35942,#35943,#35944,#35945,#35946,#35947,
#35948,#35949,#35950,#35951,#35952,#35953,#35954,#35955,#35956,#35957,#35958,
#35959,#35960,#35961,#35962,#35963,#35964,#35965,#35966,#35967,#35968,#35969,
#35970,#35971,#35972,#35973,#35974,#35975,#35976,#35977,#35978,#35979,#35980,
#35981,#35982,#35983,#35984,#35985,#35986,#35987,#35988,#35989,#35990,#35991,
#35992,#35993,#35994,#35995,#35996,#35997,#35998,#35999,#36000,#36001,#36002,
#36003,#36004,#36005,#36006,#36007,#36008,#36009,#36010,#36011,#36012,#36013,
#36014,#36015,#36016,#36017,#36018,#36019,#36020,#36021,#36022,#36023,#36024,
#36025,#36026,#36027,#36028,#36029,#36030,#36031,#36032,#36033,#36034,#36035,
#36036,#36037,#36038,#36039,#36040,#36041,#36042,#36043,#36044,#36045,#36046,
#36047,#36048,#36049,#36050,#36051,#36052,#36053,#36054,#36055,#36056,#36057,
#36058,#36059,#36060,#36061,#36062,#36063,#36064,#36065,#36066,#36067,#36068,
#36069,#36070,#36071,#36072,#36073,#36074,#36075,#36076,#36077,#36078,#36079,
#36080,#36081),.UNSPECIFIED.,.F.,.F.,(4,2,2,2,2,2,2,2,2,2,2,2,2,2,2,2,2,
2,2,2,2,2,2,2,2,2,2,2,2,2,2,2,2,2,2,2,2,2,2,2,2,2,2,2,2,2,2,2,2,2,2,2,2,
2,2,2,2,2,2,2,2,2,2,2,2,2,2,2,2,2,2,2,2,2,2,2,2,2,2,2,2,2,2,2,2,2,2,2,2,
2,2,2,2,2,2,2,4),(-1.36957890813418,-1.3469927902356,-1.28129777944894,
-1.25152420992124,-1.24871336565391,-1.24735327956401,-1.24638622643344,
-1.24541369757661,-1.24413920407232,-1.24156125744993,-1.23824079055204,
-1.21134103105977,-1.15226908486643,-1.09030224297907,-1.08659651797799,
-1.08551614712285,-1.08494363534349,-1.08443967805872,-1.08378280596457,
-1.08260835130867,-1.07718354387671,-1.0668852082195,-1.03720321283977,
-0.943982160690254,-0.927856248475247,-0.925221575850886,-0.92393113477301,
-0.922920735944101,-0.921824301649556,-0.920053931144378,-0.917957516927996,
-0.913923671016369,-0.904163212104042,-0.87096333445564,-0.768116345375349,
-0.767367264221802,-0.763564816951233,-0.762473575499792,-0.761898833557201,
-0.761394889744935,-0.760740763530272,-0.759579027392969,-0.754340217766761,
-0.669474815188671,-0.616912699767065,-0.614914589340625,-0.612703176358642,
-0.60399072960941,-0.602059251454564,-0.60080492525863,-0.599798125766958,
-0.598852927181849,-0.597159122101697,-0.591940639173503,-0.583933983672087,
-0.559813334771092,-0.530292740624415,-0.445331537452082,-0.444911824135395,
-0.440666295298508,-0.439541824557408,-0.438889228752894,-0.438328793300461,
-0.437639576422923,-0.436315066059272,-0.428056195575184,-0.410206857894458,
-0.365974713473903,-0.344819509431372,-0.31536455986921,-0.306912122631169,
-0.301949872315315,-0.297381658035824,-0.295320976351468,-0.291530083989753,
-0.287971479295353,-0.286522977077033,-0.280587581634551,-0.278731688241775,
-0.277720128875009,-0.27671520616753,-0.275752545798624,-0.274555248671002,
-0.270282797365475,-0.24423820822771,-0.22475262261072,-0.122157651599925,
-0.121329721449417,-0.117581853727496,-0.116496458495716,-0.115922778284382,
-0.115418633076506,-0.114762679901396,-0.11359321612561,-0.108246849665958,
-0.0271323909616345,-0.000962428845924314),.UNSPECIFIED.);
#206=B_SPLINE_CURVE_WITH_KNOTS('',3,(#36082,#36083,#36084,#36085,#36086,
#36087,#36088,#36089,#36090,#36091,#36092,#36093,#36094,#36095,#36096,#36097,
#36098,#36099,#36100,#36101,#36102,#36103,#36104,#36105,#36106,#36107,#36108,
#36109,#36110,#36111,#36112,#36113,#36114,#36115,#36116,#36117,#36118,#36119,
#36120,#36121,#36122,#36123,#36124,#36125,#36126,#36127,#36128,#36129,#36130,
#36131,#36132,#36133,#36134,#36135,#36136,#36137,#36138,#36139,#36140,#36141,
#36142,#36143,#36144,#36145,#36146,#36147,#36148,#36149,#36150,#36151),
 .UNSPECIFIED.,.F.,.F.,(4,3,3,3,3,3,3,3,3,3,3,3,3,3,3,3,3,3,3,3,3,3,3,4),
(327.820676619569,327.913439865354,328.006308009825,328.09923753556,328.192310868849,
328.223422501165,328.316495445441,328.409442285078,328.502290656262,328.595071160918,
328.687816483074,328.780551448175,328.873300866516,328.966149507252,329.059049947863,
329.152105843947,329.223137156638,329.316565251507,329.409866253897,329.50306464796,
329.596181863996,329.689249570431,329.782314572085,329.867228626929),
 .UNSPECIFIED.);
#207=B_SPLINE_CURVE_WITH_KNOTS('',3,(#36152,#36153,#36154,#36155,#36156,
#36157,#36158,#36159,#36160,#36161,#36162,#36163,#36164,#36165,#36166,#36167,
#36168,#36169,#36170,#36171,#36172,#36173,#36174,#36175,#36176,#36177,#36178,
#36179,#36180,#36181,#36182,#36183,#36184,#36185,#36186,#36187,#36188,#36189,
#36190,#36191,#36192,#36193,#36194,#36195,#36196,#36197,#36198,#36199,#36200,
#36201,#36202,#36203,#36204,#36205,#36206,#36207,#36208,#36209,#36210,#36211,
#36212,#36213,#36214,#36215,#36216,#36217,#36218,#36219,#36220,#36221,#36222,
#36223,#36224,#36225,#36226,#36227,#36228,#36229,#36230,#36231,#36232,#36233,
#36234,#36235,#36236,#36237,#36238,#36239,#36240,#36241,#36242,#36243,#36244,
#36245,#36246,#36247,#36248,#36249,#36250,#36251,#36252,#36253,#36254,#36255,
#36256,#36257,#36258,#36259,#36260,#36261,#36262,#36263,#36264,#36265,#36266,
#36267,#36268,#36269,#36270,#36271,#36272,#36273,#36274,#36275,#36276,#36277,
#36278,#36279,#36280,#36281,#36282,#36283,#36284,#36285,#36286,#36287,#36288,
#36289,#36290,#36291,#36292,#36293,#36294,#36295,#36296,#36297,#36298,#36299,
#36300,#36301,#36302,#36303,#36304,#36305,#36306,#36307,#36308,#36309,#36310,
#36311,#36312,#36313,#36314,#36315,#36316,#36317,#36318,#36319,#36320,#36321,
#36322,#36323,#36324,#36325,#36326,#36327,#36328,#36329,#36330,#36331,#36332,
#36333,#36334,#36335,#36336,#36337,#36338,#36339,#36340,#36341,#36342,#36343,
#36344,#36345,#36346,#36347,#36348,#36349,#36350,#36351,#36352,#36353,#36354,
#36355,#36356,#36357,#36358,#36359,#36360,#36361,#36362,#36363,#36364,#36365,
#36366,#36367,#36368,#36369,#36370,#36371,#36372,#36373,#36374,#36375,#36376,
#36377,#36378,#36379,#36380,#36381,#36382,#36383,#36384,#36385,#36386,#36387,
#36388,#36389,#36390,#36391,#36392,#36393,#36394,#36395,#36396,#36397,#36398,
#36399,#36400,#36401,#36402,#36403,#36404,#36405,#36406,#36407,#36408,#36409,
#36410,#36411,#36412,#36413,#36414,#36415,#36416,#36417,#36418,#36419,#36420,
#36421,#36422,#36423,#36424,#36425,#36426,#36427,#36428,#36429,#36430,#36431,
#36432,#36433,#36434,#36435,#36436,#36437,#36438,#36439,#36440,#36441),
 .UNSPECIFIED.,.F.,.F.,(4,2,2,2,2,2,2,2,2,2,2,2,2,2,2,2,2,2,2,2,2,2,2,2,
2,2,2,2,2,2,2,2,2,2,2,2,2,2,2,2,2,2,2,2,2,2,2,2,2,2,2,2,2,2,2,2,2,2,2,2,
2,2,2,2,2,2,2,2,2,2,2,2,2,2,2,2,2,2,2,2,2,2,2,2,2,2,2,2,2,2,2,2,2,2,2,2,
2,2,2,2,2,2,2,2,2,2,2,2,2,2,2,2,2,2,2,2,2,2,2,2,2,2,2,2,2,2,2,2,2,2,2,2,
2,2,2,2,2,2,2,2,2,2,2,2,4),(-2.69256774355998,-2.66996765412598,-2.63566077198389,
-2.62985109387609,-2.62808422619325,-2.62698018022388,-2.62596548190667,
-2.62466622748265,-2.62191704922497,-2.60331506507887,-2.60180195197674,
-2.5950314105217,-2.51817677740363,-2.48875635776303,-2.4700458035126,-2.46797349701839,
-2.46687536850086,-2.46617005212669,-2.46551300966961,-2.46498574490999,
-2.46432999646831,-2.46319213958975,-2.45881098272055,-2.45616494461932,
-2.45458776849015,-2.45322158818035,-2.35918880613108,-2.32412368799177,
-2.30801889969593,-2.30559418901551,-2.30434639556168,-2.3034358402617,
-2.30245952004982,-2.30106599394745,-2.29724499201814,-2.23938077463207,
-2.1797730545047,-2.15452365558019,-2.14467244427862,-2.14328889439957,
-2.1425873696778,-2.14202608198113,-2.1414656908577,-2.14044582356323,-2.13724668211284,
-2.08269059745371,-2.03178463617859,-2.01656255758589,-1.98624609127669,
-1.98342198169563,-1.98205845786337,-1.98109030822926,-1.98017700918456,
-1.97890913705524,-1.97638728378742,-1.95734236984911,-1.92807017578352,
-1.82572224798771,-1.82484877163046,-1.82113231211625,-1.82005042859805,
-1.81947744967867,-1.81897326980261,-1.8183163686792,-1.81714261509344,
-1.81173361166486,-1.80147795849957,-1.77218010118601,-1.66725100336038,
-1.66098835660767,-1.65909282521715,-1.65807322788367,-1.65709679229598,
-1.65600730015614,-1.65399156345612,-1.65153770550644,-1.59777846191563,
-1.50303865025389,-1.49813143157998,-1.49705063545071,-1.49635080202061,
-1.49578951729472,-1.49514463268809,-1.49402530364107,-1.4893583376198,
-1.46742676340644,-1.44241118702442,-1.38306936471926,-1.36372296834895,
-1.36003386894653,-1.33952399098644,-1.33669580755574,-1.33538124022475,
-1.33436404735965,-1.33328900351507,-1.3316102585462,-1.32964818383798,
-1.32596569920956,-1.29398676750816,-1.23402728794868,-1.17824008721575,
-1.17489067279343,-1.17385181917339,-1.1732874893112,-1.17272654098831,
-1.17203174405363,-1.17068125150515,-1.16177421683413,-1.14040191786627,
-1.03567646149139,-1.0338019612888,-1.0162034622433,-1.01349842175526,-1.0121936471515,
-1.01118107587685,-1.01009127412707,-1.00835068755469,-1.00629778474052,
-1.00237886405211,-0.992991521579222,-0.962168373499545,-0.912028914188886,
-0.855346795792154,-0.851836322314162,-0.850778213478055,-0.850210052297113,
-0.849649578891885,-0.848961582410445,-0.847643249812488,-0.839536101564362,
-0.824534978864349,-0.81011222550536,-0.799527976827988,-0.716224735434592,
-0.71417203858667,-0.693448939384863,-0.690612673562159,-0.689296705321461,
-0.688279434456218,-0.687205064749528,-0.685531850772112,-0.683575883153036,
-0.679908937780579,-0.671323053205383,-0.662358193112005),.UNSPECIFIED.);
#208=B_SPLINE_CURVE_WITH_KNOTS('',3,(#36446,#36447,#36448,#36449,#36450,
#36451,#36452,#36453,#36454,#36455,#36456,#36457,#36458,#36459,#36460,#36461,
#36462,#36463,#36464,#36465,#36466,#36467,#36468,#36469,#36470,#36471,#36472,
#36473,#36474,#36475,#36476,#36477,#36478,#36479,#36480,#36481,#36482,#36483,
#36484,#36485,#36486,#36487,#36488,#36489,#36490,#36491,#36492,#36493,#36494,
#36495,#36496,#36497,#36498,#36499,#36500,#36501,#36502,#36503,#36504,#36505,
#36506,#36507,#36508,#36509,#36510,#36511,#36512,#36513,#36514,#36515,#36516,
#36517,#36518,#36519,#36520,#36521,#36522,#36523,#36524,#36525,#36526,#36527,
#36528,#36529,#36530,#36531,#36532,#36533,#36534,#36535,#36536,#36537,#36538,
#36539,#36540,#36541,#36542,#36543,#36544,#36545,#36546,#36547,#36548,#36549,
#36550,#36551,#36552,#36553,#36554,#36555,#36556,#36557,#36558,#36559,#36560,
#36561,#36562,#36563,#36564,#36565,#36566,#36567,#36568,#36569,#36570,#36571,
#36572,#36573,#36574,#36575,#36576,#36577,#36578,#36579,#36580,#36581,#36582,
#36583,#36584,#36585,#36586,#36587,#36588,#36589,#36590,#36591,#36592,#36593,
#36594,#36595,#36596,#36597,#36598,#36599,#36600,#36601,#36602,#36603,#36604,
#36605,#36606,#36607,#36608,#36609,#36610,#36611,#36612,#36613,#36614,#36615,
#36616,#36617,#36618,#36619,#36620,#36621,#36622,#36623,#36624,#36625,#36626,
#36627,#36628,#36629,#36630,#36631,#36632,#36633,#36634,#36635,#36636,#36637,
#36638,#36639,#36640,#36641,#36642,#36643,#36644,#36645,#36646,#36647,#36648,
#36649,#36650,#36651,#36652,#36653,#36654,#36655,#36656,#36657,#36658,#36659,
#36660,#36661,#36662,#36663,#36664,#36665,#36666,#36667,#36668,#36669,#36670,
#36671,#36672,#36673,#36674,#36675,#36676,#36677,#36678,#36679,#36680,#36681,
#36682,#36683,#36684,#36685,#36686,#36687,#36688,#36689,#36690,#36691,#36692,
#36693,#36694,#36695,#36696,#36697,#36698,#36699,#36700,#36701,#36702,#36703,
#36704,#36705,#36706,#36707,#36708,#36709,#36710,#36711,#36712,#36713,#36714,
#36715,#36716,#36717,#36718,#36719,#36720,#36721,#36722,#36723,#36724,#36725,
#36726,#36727,#36728,#36729,#36730,#36731,#36732,#36733,#36734,#36735,#36736,
#36737,#36738,#36739,#36740,#36741,#36742,#36743,#36744,#36745,#36746,#36747,
#36748,#36749,#36750,#36751,#36752,#36753,#36754,#36755,#36756,#36757,#36758,
#36759,#36760,#36761,#36762,#36763,#36764,#36765),.UNSPECIFIED.,.F.,.F.,
(4,2,2,2,2,2,2,2,2,2,2,2,2,2,2,2,2,2,2,2,2,2,2,2,2,2,2,2,2,2,2,2,2,2,2,
2,2,2,2,2,2,2,2,2,2,2,2,2,2,2,2,2,2,2,2,2,2,2,2,2,2,2,2,2,2,2,2,2,2,2,2,
2,2,2,2,2,2,2,2,2,2,2,2,2,2,2,2,2,2,2,2,2,2,2,2,2,2,2,2,2,2,2,2,2,2,2,2,
2,2,2,2,2,2,2,2,2,2,2,2,2,2,2,2,2,2,2,2,2,2,2,2,2,2,2,2,2,2,2,2,2,2,2,2,
2,2,2,2,2,2,2,2,2,2,2,2,2,2,2,2,4),(-3.39861689288311,-3.39851652348514,
-3.36827023771839,-3.35602535036205,-3.34699561483257,-3.34564558857145,
-3.34494547623871,-3.34438453841218,-3.34382384136669,-3.34280163175715,
-3.33958389379969,-3.2885842080578,-3.23670937194651,-3.20258455361857,
-3.18753662018917,-3.18515915700513,-3.18390811145121,-3.18299746437958,
-3.1820232068261,-3.18063624436453,-3.17685553829957,-3.11569335840996,
-3.06628858321014,-3.03907612330084,-3.02449483328556,-3.02299860126879,
-3.02226845669901,-3.02175650609641,-3.02122078638098,-3.02047263358144,
-3.01852261416287,-2.98995595576426,-2.93814345150884,-2.89703691602468,
-2.87815288948963,-2.86470596169683,-2.86238812056126,-2.8611531181694,
-2.86014805802795,-2.8589936161466,-2.85705028863361,-2.85015738469181,
-2.84647027843376,-2.84490633688624,-2.84435319666325,-2.84294540478745,
-2.84233333239501,-2.84025219642572,-2.83875038684782,-2.83608980205276,
-2.83076484982645,-2.82380437727142,-2.80475873341698,-2.73981387447017,
-2.71432336364206,-2.70176394582584,-2.70028281793576,-2.6995556907845,
-2.69904421576642,-2.69850746631044,-2.6977555166482,-2.69578172595456,
-2.66555996394071,-2.58659208973241,-2.55615433323163,-2.54198489980303,
-2.53963623830013,-2.53839466110096,-2.53739841357727,-2.53625214003506,
-2.53429492945686,-2.52748614501906,-2.52375410452981,-2.52215215832779,
-2.52158904223564,-2.51968439490351,-2.51762162339136,-2.51649100574272,
-2.51365149540189,-2.42950603783512,-2.38122502499018,-2.3780325506904,
-2.37705572005625,-2.37643841495727,-2.37587207640918,-2.37513815952527,
-2.37355085025024,-2.36187058597992,-2.36096664951586,-2.3604068968493,
-2.32706861158301,-2.30473018161107,-2.25553440274245,-2.23129181515244,
-2.21900932405748,-2.21675210191722,-2.21553997139539,-2.21454543396193,
-2.21352870515074,-2.21164606736588,-2.20548761337272,-2.09640550436834,
-2.05726920926437,-2.05486155531322,-2.05398307363482,-2.05339179054112,
-2.05281863313086,-2.05212813671583,-2.05040691802231,-2.03473995067324,
-2.03342124108708,-2.03202265150054,-2.03068566771156,-2.00606142906807,
-1.90143488683449,-1.89518141067546,-1.89328739868671,-1.89226834765861,
-1.89127389965552,-1.89006522911721,-1.88782427961519,-1.87585350874735,
-1.85225864725069,-1.80696507188385,-1.77461275714598,-1.74769149736479,
-1.74715713969206,-1.74649456270382,-1.74540047671497,-1.73320818365469,
-1.7316218788423,-1.73087674393756,-1.73030862248911,-1.72969636994605,
-1.72872195418011,-1.72556893946214,-1.67344376111877,-1.60102359883175,
-1.59375478862298,-1.59176771332035,-1.59053921419318,-1.58953311838897,
-1.57365221254335,-1.57103011027865,-1.56974221440621,-1.56873214737932,
-1.56763435162468,-1.56585539872241,-1.56374849501562,-1.55968694774402,
-1.52200310950131,-1.43663997263336,-1.41082318375401,-1.40891624757298,
-1.40817511679209,-1.40764119906639,-1.40707106465453,-1.40630069128764,
-1.40456101703622,-1.36957890813418),.UNSPECIFIED.);
#209=B_SPLINE_CURVE_WITH_KNOTS('',3,(#36767,#36768,#36769,#36770,#36771,
#36772,#36773,#36774,#36775,#36776,#36777,#36778,#36779,#36780,#36781,#36782,
#36783,#36784,#36785,#36786,#36787,#36788,#36789,#36790,#36791,#36792,#36793,
#36794,#36795,#36796,#36797,#36798,#36799,#36800,#36801,#36802,#36803,#36804,
#36805,#36806,#36807,#36808,#36809,#36810,#36811,#36812,#36813,#36814,#36815,
#36816,#36817,#36818,#36819,#36820,#36821,#36822,#36823,#36824,#36825,#36826,
#36827,#36828,#36829,#36830,#36831,#36832,#36833,#36834,#36835,#36836,#36837,
#36838,#36839,#36840,#36841,#36842,#36843,#36844,#36845,#36846,#36847,#36848,
#36849,#36850,#36851,#36852,#36853,#36854,#36855,#36856,#36857,#36858,#36859,
#36860,#36861,#36862,#36863,#36864,#36865,#36866,#36867,#36868,#36869,#36870,
#36871,#36872,#36873,#36874,#36875,#36876,#36877,#36878,#36879,#36880,#36881,
#36882,#36883,#36884,#36885,#36886),.UNSPECIFIED.,.F.,.F.,(4,2,2,2,2,2,
2,2,2,2,2,2,2,2,2,2,2,2,2,2,2,2,2,2,2,2,2,2,2,2,2,2,2,2,2,2,2,2,2,2,2,2,
2,2,2,2,2,2,2,2,2,2,2,2,2,2,2,2,2,4),(-0.662358193112005,-0.647616252338287,
-0.614702519106575,-0.540092015397422,-0.52966865382535,-0.528285345126216,
-0.527573961132616,-0.527047617784055,-0.526471467835394,-0.525668281104276,
-0.523742771735117,-0.52108827083249,-0.492344765543757,-0.468341913570963,
-0.461357183285391,-0.455296062617719,-0.44995790422994,-0.40067392380545,
-0.370979369907446,-0.368169441813313,-0.366809275375872,-0.365841927592917,
-0.364869057430378,-0.363885777157978,-0.361736895955184,-0.351273079925747,
-0.331353298275014,-0.310014131092464,-0.216151449189928,-0.214553634804704,
-0.213070616363894,-0.210428850030765,-0.206041240766316,-0.204902546380952,
-0.204246494058574,-0.203691394797478,-0.203008260063377,-0.201713305942042,
-0.194138639463462,-0.17838142368069,-0.0853496718335142,-0.0796873961327089,
-0.072181127900674,-0.0669904556690061,-0.065437238334963,-0.0642295530878925,
-0.0628585826932495,-0.0607548061908026,-0.0602677090999533,-0.0565551932659298,
-0.052871225135495,-0.0459644942742916,-0.0440188418605291,-0.0428633689690836,
-0.041862153596501,-0.0408973949306642,-0.0396931275257946,-0.0378717285006105,
-0.0362097358738138,-0.000958175347923689),.UNSPECIFIED.);
#210=B_SPLINE_CURVE_WITH_KNOTS('',3,(#36887,#36888,#36889,#36890,#36891,
#36892,#36893,#36894,#36895,#36896,#36897,#36898,#36899,#36900,#36901,#36902,
#36903,#36904,#36905,#36906,#36907,#36908,#36909,#36910,#36911,#36912,#36913,
#36914,#36915,#36916,#36917,#36918,#36919,#36920,#36921,#36922,#36923,#36924,
#36925,#36926,#36927,#36928,#36929,#36930,#36931,#36932,#36933,#36934,#36935,
#36936,#36937,#36938,#36939,#36940,#36941,#36942,#36943,#36944,#36945,#36946,
#36947,#36948,#36949,#36950,#36951,#36952,#36953,#36954,#36955,#36956,#36957,
#36958,#36959,#36960,#36961,#36962,#36963,#36964,#36965,#36966,#36967,#36968,
#36969,#36970,#36971,#36972,#36973,#36974,#36975,#36976,#36977,#36978,#36979,
#36980,#36981,#36982,#36983,#36984,#36985,#36986,#36987,#36988,#36989,#36990,
#36991,#36992,#36993,#36994,#36995,#36996,#36997,#36998,#36999,#37000,#37001,
#37002,#37003,#37004,#37005,#37006,#37007,#37008,#37009,#37010,#37011,#37012,
#37013,#37014,#37015,#37016,#37017,#37018,#37019,#37020,#37021,#37022,#37023,
#37024,#37025,#37026,#37027,#37028),.UNSPECIFIED.,.F.,.F.,(4,3,3,3,3,3,
3,3,3,3,3,3,3,3,3,3,3,3,3,3,3,3,3,3,3,3,3,3,3,3,3,3,3,3,3,3,3,3,3,3,3,3,
3,3,3,3,3,4),(336.150413934108,336.255056496077,336.360156171105,336.465843880867,
336.522477256426,336.615550200702,336.708497040339,336.801345411524,336.894125916179,
336.986871238336,337.079606203437,337.172355621778,337.265204262513,337.358104703124,
337.451160599209,337.522191911899,337.615264856175,337.708211695812,337.801060066997,
337.893840571652,337.986585893809,338.07932085891,338.172070277251,338.264918917986,
338.357819358598,338.450875254682,338.521906567372,338.614979511648,338.707926351285,
338.80077472247,338.893555227125,338.986300549282,339.079035514383,339.171784932724,
339.264633573459,339.35753401407,339.450589910155,339.521621222845,339.614702988846,
339.711216056939,339.804052660664,339.896827067529,339.989564139875,340.082288702274,
340.175061494022,340.267863395383,340.360759758879,340.386807533587),
 .UNSPECIFIED.);
#211=B_SPLINE_CURVE_WITH_KNOTS('',3,(#37034,#37035,#37036,#37037,#37038,
#37039,#37040,#37041,#37042,#37043,#37044,#37045,#37046,#37047,#37048,#37049,
#37050,#37051,#37052,#37053,#37054,#37055,#37056,#37057,#37058,#37059,#37060,
#37061,#37062,#37063,#37064,#37065,#37066,#37067,#37068,#37069,#37070,#37071,
#37072,#37073,#37074,#37075,#37076,#37077,#37078,#37079,#37080,#37081,#37082,
#37083,#37084,#37085,#37086,#37087,#37088,#37089,#37090,#37091,#37092,#37093,
#37094,#37095,#37096,#37097,#37098,#37099,#37100,#37101,#37102,#37103,#37104,
#37105,#37106,#37107,#37108,#37109,#37110,#37111,#37112,#37113,#37114,#37115,
#37116,#37117,#37118,#37119,#37120,#37121,#37122,#37123,#37124,#37125,#37126,
#37127,#37128,#37129,#37130,#37131,#37132,#37133,#37134,#37135,#37136,#37137,
#37138,#37139,#37140,#37141,#37142,#37143,#37144,#37145,#37146,#37147,#37148,
#37149,#37150,#37151,#37152,#37153,#37154,#37155,#37156,#37157,#37158,#37159,
#37160,#37161,#37162,#37163,#37164,#37165,#37166,#37167,#37168,#37169,#37170,
#37171,#37172,#37173,#37174,#37175,#37176,#37177,#37178,#37179,#37180,#37181,
#37182,#37183,#37184,#37185,#37186,#37187,#37188,#37189,#37190,#37191,#37192,
#37193,#37194,#37195,#37196,#37197,#37198,#37199,#37200,#37201,#37202,#37203,
#37204,#37205,#37206,#37207,#37208,#37209,#37210,#37211,#37212,#37213,#37214,
#37215,#37216,#37217,#37218,#37219,#37220,#37221,#37222,#37223,#37224,#37225,
#37226,#37227,#37228,#37229),.UNSPECIFIED.,.F.,.F.,(4,2,2,2,2,2,2,2,2,2,
2,2,2,2,2,2,2,2,2,2,2,2,2,2,2,2,2,2,2,2,2,2,2,2,2,2,2,2,2,2,2,2,2,2,2,2,
2,2,2,2,2,2,2,2,2,2,2,2,2,2,2,2,2,2,2,2,2,2,2,2,2,2,2,2,2,2,2,2,2,2,2,2,
2,2,2,2,2,2,2,2,2,2,2,2,2,2,2,4),(-1.37005580231967,-1.33024580360612,-1.25976747071589,
-1.22732699997943,-1.22532367085035,-1.22456660024079,-1.22402827427647,
-1.22351707972821,-1.22279319089613,-1.2213293624247,-1.20834336199594,
-1.18312776894192,-1.1253464204192,-1.06882846069402,-1.06508845476252,
-1.06370733102199,-1.06273430621114,-1.06182252075083,-1.06056633840554,
-1.05812799461718,-1.04166633456679,-1.00224452419147,-0.947826806599637,
-0.905378626359692,-0.902642732017071,-0.901684988031656,-0.901137038948888,
-0.900629279587804,-0.899929567802679,-0.898582703622869,-0.889655800780411,
-0.868156124887796,-0.816947657365438,-0.771814035612302,-0.763968727815306,
-0.762576748009983,-0.761371407025166,-0.759881939527268,-0.757798152922224,
-0.757204406455709,-0.755598519374418,-0.754791288837574,-0.752392896527088,
-0.743795977717935,-0.741649397968903,-0.740342983766373,-0.739327099296034,
-0.738226187204517,-0.736473865355746,-0.730915072813556,-0.722236774576898,
-0.701245436118729,-0.63806871333048,-0.630014350343646,-0.582559398634975,
-0.579743080670572,-0.578774208415882,-0.57822401416436,-0.577716820865844,
-0.577021883151893,-0.576277351738385,-0.572875904693997,-0.546667491364594,
-0.503228306124239,-0.4243747544629,-0.419555190550068,-0.417849069572376,
-0.416867501604267,-0.415958154690557,-0.414721348299145,-0.413403532096508,
-0.407542562919724,-0.398252896075913,-0.368172590679002,-0.342495402157512,
-0.318402484770243,-0.260366926927176,-0.256928450608511,-0.255878891130257,
-0.255312448188767,-0.254751809138686,-0.254060907394055,-0.25332198162909,
-0.252143810125866,-0.23831051341243,-0.208329861789743,-0.196667345952084,
-0.184201381104297,-0.102044139889294,-0.0967295119488519,-0.094953789143961,
-0.0939582976298354,-0.09305183561242,-0.091842332165937,-0.090562366361816,
-0.088561293159636,-0.0740916733101073,-0.000961800400030715),
 .UNSPECIFIED.);
#212=B_SPLINE_CURVE_WITH_KNOTS('',3,(#37230,#37231,#37232,#37233,#37234,
#37235,#37236,#37237,#37238,#37239,#37240,#37241,#37242,#37243,#37244,#37245,
#37246,#37247,#37248,#37249,#37250,#37251,#37252,#37253,#37254,#37255,#37256,
#37257,#37258,#37259,#37260,#37261,#37262,#37263,#37264,#37265,#37266,#37267,
#37268,#37269,#37270,#37271,#37272,#37273,#37274,#37275,#37276,#37277,#37278,
#37279,#37280,#37281,#37282,#37283,#37284,#37285,#37286,#37287,#37288,#37289,
#37290,#37291,#37292,#37293,#37294,#37295,#37296,#37297,#37298,#37299,#37300,
#37301,#37302,#37303,#37304,#37305,#37306,#37307,#37308,#37309,#37310,#37311,
#37312,#37313,#37314,#37315,#37316,#37317,#37318,#37319,#37320,#37321,#37322,
#37323,#37324,#37325,#37326,#37327),.UNSPECIFIED.,.F.,.F.,(4,2,2,2,2,2,
2,2,2,2,2,2,2,2,2,2,2,2,2,2,2,2,2,2,2,2,2,2,2,2,2,2,2,2,2,2,2,2,2,2,2,2,
2,2,2,2,2,2,4),(-4.05896261844771,-3.99473034410128,-3.99274023828834,-3.9916739195815,
-3.99098209857863,-3.9903250601198,-3.98982122113935,-3.98924910602602,
-3.98817025384431,-3.98447649525557,-3.92166642543571,-3.90708517006878,
-3.89249015588519,-3.85066449864255,-3.83398016732095,-3.83189608600863,
-3.83058139021261,-3.82934700504211,-3.82843842056241,-3.82745669288872,
-3.82574776117373,-3.82090443335108,-3.7419525078443,-3.71863494111611,
-3.69238019397598,-3.67694520600631,-3.6720841731021,-3.66900756856252,
-3.6682853828613,-3.66760660682633,-3.66705210352949,-3.66648025187076,
-3.66540277632302,-3.66172140619556,-3.60235321536811,-3.54964971064022,
-3.51476279327677,-3.50907555017911,-3.50730945932002,-3.50620591410419,
-3.50519168646006,-3.50389304914685,-3.50114523135055,-3.48255403787029,
-3.48105085563132,-3.47649535737486,-3.46790799070911,-3.43040793471149,
-3.39861689288311),.UNSPECIFIED.);
#213=B_SPLINE_CURVE_WITH_KNOTS('',3,(#37329,#37330,#37331,#37332,#37333,
#37334,#37335,#37336,#37337,#37338,#37339,#37340,#37341,#37342,#37343,#37344,
#37345,#37346,#37347,#37348,#37349,#37350,#37351,#37352,#37353,#37354,#37355,
#37356,#37357,#37358,#37359,#37360,#37361,#37362,#37363,#37364,#37365,#37366,
#37367,#37368,#37369,#37370,#37371,#37372,#37373,#37374,#37375,#37376,#37377,
#37378,#37379,#37380,#37381,#37382,#37383,#37384,#37385,#37386,#37387,#37388,
#37389,#37390,#37391,#37392,#37393,#37394,#37395,#37396,#37397,#37398),
 .UNSPECIFIED.,.F.,.F.,(4,3,3,3,3,3,3,3,3,3,3,3,3,3,3,3,3,3,3,3,3,3,3,4),
(340.386807533587,340.479875861169,340.521335878318,340.614408822594,340.707355662231,
340.800204033416,340.892984538071,340.985729860227,341.078464825328,341.17121424367,
341.264062884405,341.356963325016,341.450019221101,341.521050533791,341.613050500166,
341.704925368368,341.796696229285,341.888409907799,341.980092335245,342.071769407751,
342.163522457848,342.255311878419,342.347246185093,342.43359924102),
 .UNSPECIFIED.);
#214=B_SPLINE_CURVE_WITH_KNOTS('',3,(#37399,#37400,#37401,#37402,#37403,
#37404,#37405,#37406,#37407,#37408,#37409,#37410,#37411,#37412,#37413,#37414,
#37415,#37416,#37417,#37418,#37419,#37420,#37421,#37422,#37423,#37424,#37425,
#37426,#37427,#37428,#37429,#37430,#37431,#37432,#37433,#37434,#37435,#37436,
#37437,#37438,#37439,#37440,#37441,#37442,#37443,#37444,#37445,#37446,#37447,
#37448,#37449,#37450,#37451,#37452,#37453,#37454,#37455,#37456,#37457,#37458,
#37459,#37460,#37461,#37462,#37463,#37464,#37465,#37466,#37467,#37468,#37469,
#37470,#37471,#37472,#37473,#37474,#37475,#37476,#37477,#37478,#37479,#37480,
#37481,#37482,#37483,#37484,#37485,#37486,#37487,#37488,#37489,#37490,#37491,
#37492,#37493,#37494,#37495,#37496,#37497,#37498,#37499,#37500,#37501,#37502,
#37503,#37504,#37505,#37506,#37507,#37508,#37509,#37510,#37511,#37512,#37513,
#37514,#37515,#37516,#37517,#37518,#37519,#37520,#37521,#37522,#37523,#37524,
#37525,#37526,#37527,#37528,#37529,#37530,#37531,#37532,#37533,#37534,#37535,
#37536,#37537,#37538,#37539,#37540,#37541,#37542,#37543,#37544,#37545,#37546,
#37547,#37548,#37549,#37550,#37551,#37552,#37553,#37554,#37555,#37556,#37557,
#37558,#37559,#37560,#37561,#37562,#37563,#37564,#37565,#37566,#37567,#37568,
#37569,#37570,#37571,#37572,#37573,#37574,#37575,#37576,#37577,#37578,#37579,
#37580,#37581,#37582,#37583,#37584,#37585,#37586,#37587,#37588,#37589,#37590,
#37591,#37592,#37593,#37594,#37595,#37596,#37597,#37598,#37599,#37600,#37601,
#37602,#37603,#37604,#37605,#37606,#37607,#37608,#37609,#37610,#37611,#37612,
#37613,#37614,#37615,#37616,#37617,#37618),.UNSPECIFIED.,.F.,.F.,(4,2,2,
2,2,2,2,2,2,2,2,2,2,2,2,2,2,2,2,2,2,2,2,2,2,2,2,2,2,2,2,2,2,2,2,2,2,2,2,
2,2,2,2,2,2,2,2,2,2,2,2,2,2,2,2,2,2,2,2,2,2,2,2,2,2,2,2,2,2,2,2,2,2,2,2,
2,2,2,2,2,2,2,2,2,2,2,2,2,2,2,2,2,2,2,2,2,2,2,2,2,2,2,2,2,2,2,2,2,2,4),
(-4.06090365677149,-4.03650691383421,-4.03503794306264,-4.03417874399937,
-4.03357297950052,-4.03304822228417,-4.0324815511079,-4.03174514766761,
-4.03014442835366,-4.01811042840495,-4.01602089160981,-4.01317938470109,
-4.00735164543766,-4.00361458512073,-3.91314864148911,-3.88841015083901,
-3.8755838029156,-3.8732995599677,-3.87208180539308,-3.87117511154732,-3.87004175666826,
-3.8681420646635,-3.86183775966219,-3.75546183898016,-3.73860015199207,
-3.72057574137164,-3.71510186543436,-3.7128600735121,-3.71119058723615,
-3.71043536912496,-3.70990277054107,-3.70937582265932,-3.70866129313091,
-3.70726500939176,-3.69649098928528,-3.69366958866057,-3.69249720088601,
-3.69169052936345,-3.68738954359101,-3.64083540286392,-3.63554893079418,
-3.62947718831727,-3.62238832983456,-3.61390976232042,-3.60334877943812,
-3.55406584824233,-3.55091995883006,-3.549532349416,-3.54850751750475,-3.54755881663269,
-3.54626804475409,-3.54307322948441,-3.50751592790596,-3.4253515613131,
-3.40466517629829,-3.39754077476591,-3.39223414559812,-3.3900430345461,
-3.38889974189793,-3.38793338559232,-3.3873277112151,-3.38676156172299,
-3.3860291877721,-3.38445023397392,-3.37298672281303,-3.37190600162919,
-3.28938725026323,-3.27789040266305,-3.24481470104432,-3.23000549721557,
-3.2276318155652,-3.22639493026571,-3.22548595260562,-3.22450519482492,
-3.22309492765316,-3.21916221855917,-3.21803989835553,-3.14422898426876,
-3.0958796153158,-3.07540150077243,-3.06963983773512,-3.06731164684711,
-3.06611677232777,-3.06511515865268,-3.06450136455486,-3.06393744727858,
-3.06320913044828,-3.06203503557193,-3.05581610874664,-2.94861772083537,
-2.90822775225174,-2.90507484152201,-2.90368603882563,-2.90266107104741,
-2.90171277293443,-2.9004233591971,-2.8972359902037,-2.86202406536336,-2.79827402491883,
-2.76610844390008,-2.74635411024007,-2.74421512002001,-2.74309167247973,
-2.74237585112871,-2.74173659961163,-2.74118706931024,-2.74062373911164,
-2.73958852076695,-2.73626490577119,-2.69269850522027),.UNSPECIFIED.);
#215=B_SPLINE_CURVE_WITH_KNOTS('',3,(#37623,#37624,#37625,#37626,#37627,
#37628,#37629,#37630,#37631,#37632,#37633,#37634,#37635,#37636,#37637,#37638,
#37639,#37640,#37641,#37642,#37643,#37644,#37645,#37646,#37647,#37648,#37649,
#37650,#37651,#37652,#37653,#37654,#37655,#37656,#37657,#37658,#37659,#37660,
#37661,#37662,#37663,#37664,#37665,#37666,#37667,#37668,#37669,#37670,#37671,
#37672,#37673,#37674,#37675,#37676,#37677,#37678,#37679,#37680,#37681,#37682,
#37683,#37684,#37685,#37686,#37687,#37688,#37689,#37690,#37691,#37692,#37693,
#37694,#37695,#37696,#37697,#37698,#37699,#37700,#37701,#37702,#37703,#37704,
#37705,#37706,#37707,#37708,#37709,#37710,#37711,#37712,#37713,#37714,#37715,
#37716,#37717,#37718,#37719,#37720,#37721,#37722,#37723,#37724,#37725,#37726,
#37727,#37728,#37729,#37730,#37731,#37732,#37733,#37734,#37735,#37736,#37737,
#37738,#37739,#37740,#37741,#37742,#37743,#37744,#37745,#37746,#37747,#37748,
#37749,#37750,#37751,#37752,#37753,#37754,#37755,#37756,#37757,#37758,#37759,
#37760,#37761,#37762,#37763,#37764,#37765,#37766,#37767,#37768,#37769,#37770,
#37771,#37772,#37773,#37774,#37775,#37776,#37777,#37778,#37779,#37780,#37781,
#37782,#37783,#37784,#37785,#37786,#37787,#37788,#37789,#37790,#37791,#37792,
#37793,#37794,#37795,#37796,#37797,#37798,#37799,#37800,#37801,#37802,#37803,
#37804,#37805,#37806,#37807,#37808,#37809,#37810,#37811,#37812,#37813,#37814,
#37815,#37816,#37817,#37818,#37819,#37820,#37821,#37822,#37823,#37824,#37825,
#37826,#37827,#37828,#37829,#37830,#37831,#37832,#37833,#37834,#37835,#37836,
#37837,#37838,#37839,#37840,#37841,#37842,#37843,#37844,#37845,#37846,#37847,
#37848,#37849,#37850,#37851,#37852,#37853,#37854,#37855,#37856,#37857,#37858,
#37859,#37860,#37861,#37862,#37863,#37864,#37865,#37866,#37867,#37868,#37869,
#37870,#37871,#37872,#37873,#37874,#37875,#37876,#37877,#37878,#37879,#37880,
#37881,#37882,#37883,#37884,#37885,#37886,#37887,#37888,#37889,#37890,#37891,
#37892,#37893,#37894,#37895,#37896,#37897,#37898,#37899,#37900),
 .UNSPECIFIED.,.F.,.F.,(4,2,2,2,2,2,2,2,2,2,2,2,2,2,2,2,2,2,2,2,2,2,2,2,
2,2,2,2,2,2,2,2,2,2,2,2,2,2,2,2,2,2,2,2,2,2,2,2,2,2,2,2,2,2,2,2,2,2,2,2,
2,2,2,2,2,2,2,2,2,2,2,2,2,2,2,2,2,2,2,2,2,2,2,2,2,2,2,2,2,2,2,2,2,2,2,2,
2,2,2,2,2,2,2,2,2,2,2,2,2,2,2,2,2,2,2,2,2,2,2,2,2,2,2,2,2,2,2,2,2,2,2,2,
2,2,2,2,2,2,4),(-3.40025096654499,-3.38155611820142,-3.34393882372037,-3.33338972967109,
-3.32692255626889,-3.32556558839844,-3.32430049310195,-3.32338749826037,
-3.32241809333174,-3.32077322908984,-3.31636102715128,-3.24562691126371,
-3.19082983785927,-3.17272910773228,-3.16445210494803,-3.16313055408729,
-3.16243620764226,-3.16192910254588,-3.16137866363258,-3.16040849738475,
-3.15758358424338,-3.11299468621227,-3.05431965029234,-3.0317508094232,
-3.00576699987662,-3.00286353359999,-3.00150536581751,-3.00048499657265,
-2.99952788218792,-2.99820600957199,-2.99483136415524,-2.94894244250121,
-2.89622382141443,-2.84403171867342,-2.8408854818025,-2.83991107487678,
-2.8392941635221,-2.83872726243023,-2.83799135228704,-2.83639480412127,
-2.82449631257564,-2.82222013743134,-2.82184149812791,-2.81969096127196,
-2.81854163675169,-2.81644671374313,-2.81281856171323,-2.80060771051165,
-2.72662369446285,-2.68725352174405,-2.68095192020027,-2.67911788794578,
-2.6779987177767,-2.67698774275303,-2.67569596828261,-2.67305648717332,
-2.6568455363385,-2.65244139698332,-2.64842184033646,-2.60312270076675,
-2.52156968367137,-2.51917408748517,-2.51741295251979,-2.51664051842196,
-2.51606705145154,-2.51553733472715,-2.51481289099728,-2.5133787543379,
-2.50157483587094,-2.49995370585496,-2.49854492846162,-2.41047518669012,
-2.36112641174212,-2.35721605464612,-2.35568601513499,-2.35463338275629,
-2.35360328475375,-2.3523633096534,-2.34927425952295,-2.3208035861809,-2.25472255978626,
-2.19985466633593,-2.19506996259308,-2.19394143822851,-2.19329452603415,
-2.19273346699345,-2.19203646784877,-2.19096474209843,-2.18617002164156,
-2.09293742067761,-2.0525817079453,-2.03586283693807,-2.03341569198889,
-2.03216311326978,-2.03125181606283,-2.03013943624266,-2.02833566801064,
-2.02219060757186,-1.98462458108777,-1.90098551366252,-1.8732857636046,
-1.87134772420953,-1.8706012255069,-1.87006571270415,-1.86949608198602,
-1.86873008676845,-1.86701565432522,-1.82507400083735,-1.72837526106657,
-1.72631118180589,-1.71279971177686,-1.71055580244768,-1.7092205919148,
-1.70820020408421,-1.70711188946695,-1.70541606933145,-1.70032140206661,
-1.64002545778456,-1.59451200929741,-1.55133546227645,-1.54856177637091,
-1.54759881508932,-1.54704983219648,-1.5465423747457,-1.54584498764939,
-1.544593531872,-1.54297319025427,-1.50379242476819,-1.43156030977308,-1.41971013121211,
-1.39077942276331,-1.38771854392708,-1.38646243209228,-1.38552212969164,
-1.38448958308601,-1.38306102914433,-1.37976380560742,-1.37526717837525,
-1.37005580231967),.UNSPECIFIED.);
#216=B_SPLINE_CURVE_WITH_KNOTS('',3,(#37901,#37902,#37903,#37904,#37905,
#37906,#37907,#37908,#37909,#37910,#37911,#37912,#37913,#37914,#37915,#37916,
#37917,#37918,#37919,#37920,#37921,#37922,#37923,#37924,#37925,#37926,#37927,
#37928,#37929,#37930,#37931,#37932,#37933,#37934,#37935,#37936,#37937,#37938,
#37939,#37940,#37941,#37942,#37943,#37944,#37945,#37946,#37947,#37948,#37949,
#37950,#37951,#37952,#37953,#37954,#37955,#37956,#37957,#37958,#37959,#37960,
#37961,#37962,#37963,#37964,#37965,#37966,#37967,#37968,#37969,#37970,#37971,
#37972,#37973,#37974,#37975,#37976,#37977,#37978,#37979,#37980,#37981,#37982,
#37983,#37984,#37985,#37986,#37987,#37988,#37989,#37990,#37991,#37992,#37993,
#37994,#37995,#37996,#37997,#37998,#37999,#38000,#38001,#38002,#38003,#38004,
#38005,#38006,#38007,#38008,#38009,#38010,#38011,#38012,#38013,#38014,#38015,
#38016,#38017,#38018,#38019,#38020,#38021,#38022,#38023,#38024,#38025,#38026,
#38027,#38028,#38029,#38030,#38031,#38032,#38033,#38034,#38035,#38036,#38037,
#38038,#38039,#38040,#38041,#38042,#38043,#38044,#38045,#38046,#38047,#38048,
#38049,#38050,#38051,#38052,#38053,#38054,#38055,#38056,#38057,#38058,#38059,
#38060,#38061,#38062,#38063,#38064,#38065,#38066,#38067,#38068,#38069,#38070,
#38071,#38072,#38073,#38074,#38075,#38076,#38077,#38078,#38079,#38080,#38081,
#38082,#38083,#38084,#38085,#38086,#38087,#38088,#38089,#38090,#38091,#38092,
#38093,#38094,#38095,#38096,#38097,#38098,#38099,#38100,#38101,#38102,#38103,
#38104,#38105,#38106,#38107,#38108,#38109,#38110,#38111,#38112,#38113,#38114,
#38115,#38116,#38117,#38118,#38119,#38120,#38121,#38122,#38123,#38124,#38125,
#38126,#38127,#38128,#38129,#38130,#38131,#38132,#38133,#38134,#38135,#38136,
#38137,#38138,#38139,#38140,#38141,#38142,#38143,#38144,#38145,#38146,#38147,
#38148,#38149,#38150,#38151,#38152,#38153,#38154,#38155,#38156,#38157,#38158,
#38159,#38160,#38161,#38162,#38163,#38164,#38165,#38166,#38167,#38168),
 .UNSPECIFIED.,.F.,.F.,(4,2,2,2,2,2,2,2,2,2,2,2,2,2,2,2,2,2,2,2,2,2,2,2,
2,2,2,2,2,2,2,2,2,2,2,2,2,2,2,2,2,2,2,2,2,2,2,2,2,2,2,2,2,2,2,2,2,2,2,2,
2,2,2,2,2,2,2,2,2,2,2,2,2,2,2,2,2,2,2,2,2,2,2,2,2,2,2,2,2,2,2,2,2,2,2,2,
2,2,2,2,2,2,2,2,2,2,2,2,2,2,2,2,2,2,2,2,2,2,2,2,2,2,2,2,2,2,2,2,2,2,2,2,
2,4),(-2.69269850522027,-2.68332553922718,-2.62048867816285,-2.59632731631076,
-2.58408716150558,-2.58183230508675,-2.58062075988093,-2.5796263475247,
-2.57860943570164,-2.57672555205305,-2.57055566976022,-2.46436782869153,
-2.42211956853202,-2.42063008724243,-2.41976246224811,-2.4189892401686,
-2.41842592393518,-2.41789872937814,-2.41718339976749,-2.41578417533183,
-2.40493560905856,-2.4033324964891,-2.40248250410415,-2.40175049514704,
-2.4013347787392,-2.40050076174969,-2.39841032175249,-2.39694335998903,
-2.35780648129755,-2.32953269623204,-2.2967733773997,-2.27315221088142,
-2.26116775899695,-2.25892597961488,-2.25771708355076,-2.2567225656347,
-2.25570354382474,-2.2538098852611,-2.24756000256042,-2.14040209746362,
-2.11671385998837,-2.10582211329231,-2.09787424955118,-2.09656296193655,
-2.09587653677614,-2.09537040445473,-2.09481620813607,-2.09400150830972,
-2.09161241384246,-2.05328129214903,-2.03202133373016,-1.9994680771561,
-1.94036227393768,-1.9367476625031,-1.93538667394232,-1.93441924155934,
-1.93350573989631,-1.93223618999126,-1.92970593647032,-1.91036996899143,
-1.88032205027464,-1.78928044733773,-1.77549282496975,-1.77399511399825,
-1.77325470213926,-1.77272085456881,-1.77215035657759,-1.77137875153678,
-1.76963317913417,-1.72844597672819,-1.62047994688679,-1.61435166694624,
-1.61247233333348,-1.61145609413407,-1.61047171524352,-1.60928715236349,
-1.60801785257924,-1.60604186074277,-1.56812619943236,-1.47413220014332,
-1.46575333273969,-1.46286235505579,-1.45213912180586,-1.4507442975097,
-1.45002997238769,-1.44950290967792,-1.44892746907769,-1.44812791533062,
-1.44622351683734,-1.44360551374404,-1.41558822615915,-1.29654548678039,
-1.29096791044087,-1.28915761351063,-1.28815535415416,-1.28716999357543,
-1.28596268773031,-1.28466191600338,-1.28261117468599,-1.22743010036261,
-1.13313105828487,-1.12830314847934,-1.12722889181132,-1.12653118451408,
-1.12597018646404,-1.12532404820821,-1.12419862339508,-1.11945171417449,
-1.07695250517436,-0.974114835876923,-0.96797050404025,-0.966089325860205,
-0.965072762440275,-0.964088967484302,-0.962905089844943,-0.9616369257758,
-0.959663549564539,-0.922140185093852,-0.829430174877555,-0.824070437235926,
-0.820254203183707,-0.818885882692225,-0.818470077000964,-0.817696775710925,
-0.805842762805436,-0.804407170265072,-0.803682449885206,-0.803152749727536,
-0.802579520431882,-0.801791897144688,-0.799956159517104,-0.797456091475399,
-0.708716229361596,-0.662248326428725),.UNSPECIFIED.);
#217=B_SPLINE_CURVE_WITH_KNOTS('',3,(#38174,#38175,#38176,#38177,#38178,
#38179,#38180,#38181,#38182,#38183,#38184,#38185,#38186,#38187,#38188,#38189,
#38190,#38191,#38192,#38193,#38194,#38195,#38196,#38197,#38198,#38199,#38200,
#38201,#38202,#38203,#38204,#38205,#38206,#38207,#38208,#38209,#38210,#38211,
#38212,#38213,#38214,#38215,#38216,#38217,#38218,#38219,#38220,#38221,#38222,
#38223,#38224,#38225,#38226,#38227,#38228,#38229,#38230,#38231,#38232,#38233,
#38234,#38235,#38236,#38237,#38238,#38239,#38240,#38241,#38242,#38243,#38244,
#38245,#38246,#38247,#38248,#38249,#38250,#38251,#38252,#38253,#38254,#38255,
#38256,#38257,#38258,#38259,#38260,#38261,#38262,#38263,#38264,#38265,#38266,
#38267,#38268,#38269,#38270,#38271,#38272,#38273,#38274,#38275,#38276,#38277,
#38278,#38279,#38280,#38281,#38282,#38283,#38284,#38285,#38286,#38287,#38288,
#38289,#38290,#38291,#38292,#38293,#38294,#38295,#38296,#38297,#38298,#38299,
#38300,#38301,#38302,#38303,#38304,#38305,#38306,#38307,#38308,#38309,#38310,
#38311,#38312,#38313,#38314,#38315,#38316,#38317,#38318,#38319,#38320,#38321,
#38322,#38323,#38324,#38325,#38326,#38327,#38328,#38329,#38330,#38331,#38332,
#38333,#38334,#38335,#38336,#38337,#38338,#38339,#38340,#38341,#38342,#38343,
#38344,#38345,#38346,#38347,#38348,#38349,#38350,#38351,#38352,#38353,#38354,
#38355,#38356,#38357,#38358,#38359,#38360,#38361,#38362,#38363,#38364,#38365,
#38366,#38367,#38368,#38369,#38370,#38371),.UNSPECIFIED.,.F.,.F.,(4,2,2,
2,2,2,2,2,2,2,2,2,2,2,2,2,2,2,2,2,2,2,2,2,2,2,2,2,2,2,2,2,2,2,2,2,2,2,2,
2,2,2,2,2,2,2,2,2,2,2,2,2,2,2,2,2,2,2,2,2,2,2,2,2,2,2,2,2,2,2,2,2,2,2,2,
2,2,2,2,2,2,2,2,2,2,2,2,2,2,2,2,2,2,2,2,2,2,2,4),(-1.36942377060857,-1.36559877502083,
-1.36362053690649,-1.36286760451683,-1.36233039018199,-1.36181867556833,
-1.36109153358451,-1.35961161092896,-1.34697148556379,-1.32152889274019,
-1.25630302805756,-1.23550284582958,-1.20615021107675,-1.20334845643425,
-1.20199030829124,-1.20102351557963,-1.20010949529152,-1.19883743689666,
-1.19645200889229,-1.18007908179885,-1.14099979542526,-1.08255363300622,
-1.05156743024829,-1.04963064631632,-1.041767365488,-1.04037537799865,-1.03966255684123,
-1.03910015562647,-1.03846410042036,-1.03740593381582,-1.03344020507378,
-1.00528182224472,-0.948729506704858,-0.884482542479156,-0.880533412635055,
-0.879120270479407,-0.878138427624577,-0.87722915907992,-0.875992965776401,
-0.873687147348508,-0.86070872706831,-0.836588400741853,-0.774685107884237,
-0.729638658213808,-0.719017702671611,-0.717626699217039,-0.716913323361167,
-0.716386468347071,-0.715810748423445,-0.715238985858369,-0.71381951318371,
-0.702624361397662,-0.684518239076959,-0.636044977739776,-0.562586983107782,
-0.557831569357439,-0.556134771667546,-0.55515507034229,-0.55424525423192,
-0.553004448865848,-0.551681088994354,-0.545732871049633,-0.511244622740464,
-0.458784160366601,-0.398706302005173,-0.39520880920484,-0.394152211316115,
-0.393584342815754,-0.393023824211013,-0.392335289717044,-0.391599661830646,
-0.388334734703975,-0.383085280962421,-0.37181597524073,-0.342917468096281,
-0.318447543880378,-0.239659998788011,-0.238856093904025,-0.234661294348008,
-0.233050789557542,-0.232088089921339,-0.231070665969788,-0.229731420928208,
-0.22827189523805,-0.225842373078562,-0.208854241193399,-0.168107931902686,
-0.1537095578637,-0.139288922174846,-0.0761971701861116,-0.0723180763900793,
-0.071218267628141,-0.0706417107919776,-0.0701376726271744,-0.0694854789227201,
-0.068800613824145,-0.0677512400895286,-0.0658053860028119,-0.000961407761673223),
 .UNSPECIFIED.);
#218=B_SPLINE_CURVE_WITH_KNOTS('',3,(#38372,#38373,#38374,#38375,#38376,
#38377,#38378,#38379,#38380,#38381,#38382,#38383,#38384,#38385,#38386,#38387,
#38388,#38389,#38390,#38391,#38392,#38393,#38394,#38395,#38396,#38397,#38398,
#38399,#38400,#38401,#38402,#38403,#38404,#38405,#38406,#38407,#38408,#38409,
#38410,#38411,#38412,#38413,#38414,#38415,#38416,#38417,#38418,#38419,#38420,
#38421,#38422,#38423,#38424,#38425,#38426,#38427,#38428,#38429,#38430,#38431,
#38432,#38433,#38434,#38435,#38436,#38437,#38438,#38439,#38440,#38441,#38442,
#38443,#38444,#38445,#38446,#38447,#38448,#38449,#38450,#38451,#38452,#38453,
#38454,#38455,#38456,#38457,#38458,#38459,#38460,#38461,#38462,#38463,#38464,
#38465,#38466,#38467),.UNSPECIFIED.,.F.,.F.,(4,2,2,2,2,2,2,2,2,2,2,2,2,
2,2,2,2,2,2,2,2,2,2,2,2,2,2,2,2,2,2,2,2,2,2,2,2,2,2,2,2,2,2,2,2,2,2,4),
(-4.06158259407951,-3.98902691859257,-3.97454587785814,-3.9725398664761,
-3.97125785962089,-3.97004690679561,-3.9691403957768,-3.96814588573345,
-3.96637471630796,-3.96109284372864,-3.87929163028354,-3.86674666089183,
-3.85498350879111,-3.82472061324442,-3.81089576516494,-3.80972124900028,
-3.80898388511476,-3.80829412993813,-3.80773361512119,-3.80716660628314,
-3.80611403914643,-3.80264980125633,-3.74480708704601,-3.72336325636554,
-3.70208068315013,-3.66634034905488,-3.65612899566236,-3.64982237700015,
-3.6484754502877,-3.64721762777941,-3.64630567426265,-3.64533343104751,
-3.64395501111696,-3.64023191138441,-3.63871254260851,-3.56437279448885,
-3.56026095102796,-3.51627888696708,-3.48859664585569,-3.4864713954419,
-3.48582545250585,-3.48520074651943,-3.48463611537343,-3.48391577138633,
-3.48240037145606,-3.47244749653559,-3.42701327748576,-3.40025096654499),
 .UNSPECIFIED.);
#219=B_SPLINE_CURVE_WITH_KNOTS('',3,(#38469,#38470,#38471,#38472,#38473,
#38474,#38475,#38476,#38477,#38478,#38479,#38480,#38481,#38482,#38483,#38484,
#38485,#38486,#38487,#38488,#38489,#38490,#38491,#38492,#38493,#38494,#38495,
#38496,#38497,#38498,#38499,#38500,#38501,#38502,#38503,#38504,#38505,#38506,
#38507,#38508,#38509,#38510,#38511,#38512,#38513,#38514,#38515,#38516,#38517,
#38518,#38519,#38520,#38521,#38522,#38523,#38524,#38525,#38526,#38527,#38528,
#38529,#38530,#38531,#38532,#38533,#38534,#38535,#38536,#38537,#38538,#38539,
#38540,#38541,#38542,#38543,#38544,#38545,#38546,#38547,#38548,#38549,#38550,
#38551,#38552,#38553,#38554),.UNSPECIFIED.,.F.,.F.,(4,2,2,2,2,2,2,2,2,2,
2,2,2,2,2,2,2,2,2,2,2,2,2,2,2,2,2,2,2,2,2,2,2,2,2,2,2,2,2,2,2,2,4),(-0.662248326428725,
-0.647939429323128,-0.644191399751803,-0.642809200227694,-0.641836019189344,
-0.64084355046288,-0.639573179308982,-0.638185328386442,-0.635927432817154,
-0.631463961838477,-0.587045294089171,-0.493121853742009,-0.482671181599808,
-0.481286865928025,-0.480575244506379,-0.480048863167519,-0.47947281359014,
-0.47867001851113,-0.476746637390012,-0.474095783395336,-0.445424450922808,
-0.379073631685477,-0.324539434749613,-0.321065826510201,-0.319727597728636,
-0.318766209030686,-0.317768618264209,-0.316463897247218,-0.315028611600712,
-0.312657281494422,-0.265986767841822,-0.163398479016872,-0.162571639898673,
-0.158822646186717,-0.157737070370335,-0.157163324557509,-0.156659138392786,
-0.156003154520508,-0.154833700610107,-0.149488436632919,-0.06850952425481,
-0.0127049774281039,-0.000961729954404432),.UNSPECIFIED.);
#220=B_SPLINE_CURVE_WITH_KNOTS('',3,(#38555,#38556,#38557,#38558,#38559,
#38560,#38561,#38562,#38563,#38564,#38565,#38566,#38567,#38568,#38569,#38570,
#38571,#38572,#38573,#38574,#38575,#38576,#38577,#38578,#38579,#38580,#38581,
#38582,#38583,#38584,#38585,#38586,#38587,#38588,#38589,#38590,#38591,#38592,
#38593,#38594,#38595,#38596,#38597,#38598,#38599,#38600,#38601,#38602,#38603,
#38604,#38605,#38606,#38607,#38608,#38609,#38610,#38611,#38612,#38613,#38614,
#38615,#38616,#38617,#38618,#38619,#38620,#38621,#38622,#38623,#38624,#38625,
#38626,#38627,#38628,#38629,#38630,#38631,#38632,#38633,#38634,#38635,#38636,
#38637,#38638,#38639,#38640,#38641,#38642,#38643,#38644,#38645,#38646,#38647,
#38648,#38649,#38650,#38651,#38652,#38653,#38654,#38655,#38656,#38657,#38658,
#38659,#38660,#38661,#38662,#38663,#38664,#38665,#38666,#38667,#38668,#38669,
#38670,#38671,#38672,#38673,#38674,#38675,#38676,#38677,#38678,#38679,#38680,
#38681,#38682,#38683,#38684,#38685,#38686,#38687,#38688,#38689,#38690,#38691,
#38692,#38693,#38694,#38695,#38696),.UNSPECIFIED.,.F.,.F.,(4,3,3,3,3,3,
3,3,3,3,3,3,3,3,3,3,3,3,3,3,3,3,3,3,3,3,3,3,3,3,3,3,3,3,3,3,3,3,3,3,3,3,
3,3,3,3,3,4),(354.999969855647,355.096451305071,355.193049126282,355.28986323818,
355.3867981232,355.483945074556,355.51705571041,355.610128654686,355.703075494323,
355.795923865508,355.888704370163,355.981449692319,356.074184657421,356.166934075762,
356.259782716497,356.352683157109,356.445739053193,356.516770365883,356.609843310159,
356.702790149796,356.795638520981,356.888419025636,356.981164347793,357.073899312894,
357.166648731235,357.25949737197,357.352397812582,357.445453708666,357.516485021356,
357.609557965632,357.702504805269,357.795353176454,357.888133681109,357.980879003266,
358.073613968367,358.166363386708,358.259212027443,358.352112468055,358.445168364139,
358.516199676829,358.609250019074,358.70218389026,358.795026308277,358.887802206273,
358.980552664654,359.073285531874,359.166063108531,359.23634059125),
 .UNSPECIFIED.);
#221=B_SPLINE_CURVE_WITH_KNOTS('',3,(#38701,#38702,#38703,#38704,#38705,
#38706,#38707,#38708,#38709,#38710,#38711,#38712,#38713,#38714,#38715,#38716,
#38717,#38718,#38719,#38720,#38721,#38722,#38723,#38724,#38725,#38726,#38727,
#38728,#38729,#38730,#38731,#38732,#38733,#38734,#38735,#38736,#38737,#38738,
#38739,#38740,#38741,#38742,#38743,#38744,#38745,#38746,#38747,#38748,#38749,
#38750,#38751,#38752,#38753,#38754,#38755,#38756,#38757,#38758,#38759,#38760,
#38761,#38762,#38763,#38764,#38765,#38766,#38767,#38768,#38769,#38770,#38771,
#38772,#38773,#38774,#38775,#38776,#38777,#38778,#38779,#38780,#38781,#38782,
#38783,#38784,#38785,#38786,#38787,#38788,#38789,#38790,#38791,#38792,#38793,
#38794,#38795,#38796,#38797,#38798,#38799,#38800,#38801,#38802,#38803,#38804,
#38805,#38806,#38807,#38808,#38809,#38810,#38811,#38812,#38813,#38814,#38815,
#38816,#38817,#38818,#38819,#38820,#38821,#38822,#38823,#38824,#38825,#38826,
#38827,#38828,#38829,#38830,#38831,#38832,#38833,#38834,#38835,#38836,#38837,
#38838,#38839,#38840,#38841,#38842,#38843,#38844,#38845,#38846,#38847,#38848,
#38849,#38850,#38851,#38852,#38853,#38854,#38855,#38856,#38857,#38858,#38859,
#38860,#38861,#38862,#38863,#38864,#38865,#38866,#38867,#38868,#38869,#38870,
#38871,#38872,#38873,#38874,#38875,#38876,#38877,#38878,#38879,#38880,#38881,
#38882,#38883,#38884,#38885,#38886,#38887,#38888,#38889,#38890,#38891,#38892,
#38893,#38894,#38895,#38896,#38897,#38898,#38899,#38900,#38901,#38902,#38903,
#38904,#38905,#38906,#38907,#38908,#38909,#38910,#38911,#38912,#38913,#38914,
#38915,#38916,#38917,#38918,#38919,#38920,#38921,#38922,#38923,#38924,#38925,
#38926,#38927,#38928,#38929,#38930,#38931,#38932,#38933,#38934,#38935,#38936,
#38937,#38938,#38939,#38940,#38941,#38942,#38943,#38944,#38945,#38946,#38947,
#38948,#38949,#38950,#38951,#38952,#38953,#38954,#38955,#38956,#38957,#38958),
 .UNSPECIFIED.,.F.,.F.,(4,2,2,2,2,2,2,2,2,2,2,2,2,2,2,2,2,2,2,2,2,2,2,2,
2,2,2,2,2,2,2,2,2,2,2,2,2,2,2,2,2,2,2,2,2,2,2,2,2,2,2,2,2,2,2,2,2,2,2,2,
2,2,2,2,2,2,2,2,2,2,2,2,2,2,2,2,2,2,2,2,2,2,2,2,2,2,2,2,2,2,2,2,2,2,2,2,
2,2,2,2,2,2,2,2,2,2,2,2,2,2,2,2,2,2,2,2,2,2,2,2,2,2,2,2,2,2,2,2,4),(-3.39966259726345,
-3.34930942753569,-3.31835551769945,-3.30796621344053,-3.30250707491916,
-3.30133043712181,-3.30067315117589,-3.30016925944657,-3.29959723048155,
-3.29851896952887,-3.29483097986264,-3.29391970540771,-3.21843406511585,
-3.17019305653192,-3.15241167225209,-3.14610953319681,-3.14319626496594,
-3.14087828645481,-3.13965918791189,-3.1386646026662,-3.13752068832588,
-3.13557426401416,-3.12886346311778,-3.12507957653716,-3.1212290071838,
-3.12074785294598,-3.11864305497853,-3.02730976720726,-2.98428094326636,
-2.97951874705186,-2.97839235471009,-2.97774611860352,-2.9771853137359,
-2.97648820486979,-2.97541552952473,-2.97060467065372,-2.87750633584063,
-2.82270276397698,-2.81998370831462,-2.8177945207525,-2.8166026652889,-2.81559853805938,
-2.81458194984785,-2.81269990762598,-2.80654611364521,-2.70052542053249,
-2.66105566960581,-2.65641638241295,-2.65529959453582,-2.65465545496267,
-2.65409437674978,-2.65339423272582,-2.65231190760501,-2.647381515798,-2.55198711800444,
-2.49953759627428,-2.49684569794216,-2.49467151645231,-2.49348430031026,
-2.49248973891235,-2.49147256993718,-2.4895879043092,-2.48341298356492,
-2.38029504463951,-2.33429109004294,-2.33256748712646,-2.33179998638969,
-2.33123027725755,-2.33069547636651,-2.32995116947577,-2.32802544855145,
-2.3010694682733,-2.21146565449179,-2.18667608153743,-2.17392844281765,
-2.17164750401975,-2.17043020308167,-2.16942589087345,-2.16840953665211,
-2.16652915723888,-2.16039072651125,-2.05471432427409,-2.03046112007357,
-2.02927466374306,-2.02588143178242,-2.02483194507878,-2.01111686453133,
-2.00962147771019,-2.00888170501469,-2.00834808070855,-2.00777758873436,
-2.00700559963059,-2.00525750351294,-2.00290604398428,-1.97970645259788,
-1.95470635180935,-1.89978433188292,-1.89427779205259,-1.87763177298475,
-1.87138136987099,-1.85176289547256,-1.84925018966872,-1.84796483708003,
-1.84701730856382,-1.84599103934444,-1.84459668839262,-1.84141487999575,
-1.79845660312388,-1.699760571375,-1.6880232200218,-1.68643309421035,-1.68569840762128,
-1.68513170402537,-1.68451423739202,-1.68353764249069,-1.68035029188592,
-1.6322065708271,-1.54782539366473,-1.54455141498501,-1.52839826913049,
-1.52576155176459,-1.5244703805501,-1.5234595343635,-1.52234015515182,-1.52050498035741,
-1.51419121737665,-1.47468704401601,-1.3960678521665,-1.36942377060857),
 .UNSPECIFIED.);
#222=B_SPLINE_CURVE_WITH_KNOTS('',3,(#38960,#38961,#38962,#38963,#38964,
#38965,#38966,#38967,#38968,#38969,#38970,#38971,#38972,#38973,#38974,#38975,
#38976,#38977,#38978,#38979,#38980,#38981,#38982,#38983,#38984,#38985,#38986,
#38987,#38988,#38989,#38990,#38991,#38992,#38993,#38994,#38995,#38996,#38997,
#38998,#38999,#39000,#39001,#39002,#39003,#39004,#39005,#39006,#39007,#39008,
#39009,#39010,#39011,#39012,#39013,#39014,#39015,#39016,#39017,#39018,#39019,
#39020,#39021,#39022,#39023,#39024,#39025,#39026,#39027,#39028,#39029),
 .UNSPECIFIED.,.F.,.F.,(4,3,3,3,3,3,3,3,3,3,3,3,3,3,3,3,3,3,3,3,3,3,3,4),
(359.23634059125,359.329226379691,359.422570355996,359.515914332302,359.608987276577,
359.701934116215,359.7947824874,359.887562992055,359.980308314211,360.073043279312,
360.165792697653,360.258641338388,360.351541779,360.444597675084,360.515628987774,
360.61156975962,360.703295257999,360.794935418517,360.886516342147,360.978064063546,
361.069633525802,361.161216235208,361.252875332287,361.283155162539),
 .UNSPECIFIED.);
#223=B_SPLINE_CURVE_WITH_KNOTS('',3,(#39030,#39031,#39032,#39033,#39034,
#39035,#39036,#39037,#39038,#39039,#39040,#39041,#39042,#39043,#39044,#39045,
#39046,#39047,#39048,#39049,#39050,#39051,#39052,#39053,#39054,#39055,#39056,
#39057,#39058,#39059,#39060,#39061,#39062,#39063,#39064,#39065,#39066,#39067,
#39068,#39069,#39070,#39071,#39072,#39073,#39074,#39075,#39076,#39077,#39078,
#39079,#39080,#39081,#39082,#39083,#39084,#39085,#39086,#39087,#39088,#39089,
#39090,#39091,#39092,#39093,#39094,#39095,#39096,#39097,#39098,#39099,#39100,
#39101,#39102,#39103,#39104,#39105,#39106,#39107,#39108,#39109,#39110,#39111,
#39112,#39113,#39114,#39115,#39116,#39117,#39118,#39119,#39120,#39121,#39122,
#39123,#39124,#39125,#39126,#39127,#39128,#39129,#39130,#39131,#39132,#39133,
#39134,#39135,#39136,#39137,#39138,#39139,#39140,#39141,#39142,#39143,#39144,
#39145,#39146,#39147,#39148,#39149,#39150,#39151,#39152,#39153,#39154,#39155,
#39156,#39157,#39158,#39159,#39160,#39161,#39162,#39163,#39164,#39165,#39166,
#39167,#39168,#39169,#39170,#39171,#39172,#39173,#39174,#39175,#39176,#39177,
#39178,#39179,#39180,#39181,#39182,#39183,#39184,#39185,#39186,#39187,#39188,
#39189,#39190,#39191,#39192,#39193,#39194,#39195,#39196,#39197,#39198,#39199,
#39200,#39201,#39202,#39203,#39204,#39205,#39206,#39207,#39208,#39209,#39210,
#39211,#39212,#39213,#39214,#39215,#39216,#39217,#39218,#39219,#39220,#39221,
#39222,#39223,#39224,#39225),.UNSPECIFIED.,.F.,.F.,(4,2,2,2,2,2,2,2,2,2,
2,2,2,2,2,2,2,2,2,2,2,2,2,2,2,2,2,2,2,2,2,2,2,2,2,2,2,2,2,2,2,2,2,2,2,2,
2,2,2,2,2,2,2,2,2,2,2,2,2,2,2,2,2,2,2,2,2,2,2,2,2,2,2,2,2,2,2,2,2,2,2,2,
2,2,2,2,2,2,2,2,2,2,2,2,2,2,2,4),(-4.05985780112435,-3.9949188893063,-3.9899681927845,
-3.98788643122196,-3.98678473053978,-3.9860779547586,-3.98541016780942,
-3.98490562802089,-3.9842559994703,-3.98314418791168,-3.97902447548922,
-3.9112993717401,-3.8976739749491,-3.88421896989649,-3.84577120163737,-3.82906339179991,
-3.82694368550262,-3.82561383237739,-3.82436839526673,-3.82345818728114,
-3.82248093233968,-3.82079566012486,-3.81611704303792,-3.74261159482878,
-3.71880170592077,-3.69371240009228,-3.6733179866591,-3.66756832562051,
-3.66406807968174,-3.66331705850079,-3.66261750579369,-3.662056414542,-3.66141171689633,
-3.66032105294822,-3.65640508645385,-3.59218123965039,-3.54245757420453,
-3.50987479613646,-3.50402667469848,-3.50271028705841,-3.50147457377119,
-3.50056554787565,-3.49958386064442,-3.49817075923631,-3.49422057437485,
-3.42993477408235,-3.39613394437811,-3.3639375637965,-3.34983104687737,
-3.34448532492474,-3.34117476045616,-3.34043623779244,-3.33974567376057,
-3.33918519144089,-3.33861880583541,-3.33756906627434,-3.33412769522635,
-3.27949665326839,-3.2315054257684,-3.19736196418451,-3.18229363118905,
-3.17992323803511,-3.17867341078234,-3.17776263876735,-3.17678728865184,
-3.17539716436698,-3.17159796048124,-3.11418552568979,-3.06090380541502,
-3.03377434140109,-3.02693480855402,-3.01891594981985,-3.01760520781451,
-3.01691326496517,-3.01640654066568,-3.01585515188944,-3.01487982933241,
-3.01201908616973,-2.96731958466446,-2.90687826760608,-2.88556733372441,
-2.8602803746977,-2.85738732761159,-2.85603039769741,-2.85501042254602,
-2.8540532863847,-2.85273076520681,-2.84935115540602,-2.80307511721189,
-2.73410379436719,-2.70772127423793,-2.6962464668446,-2.69481911634679,
-2.69410274546337,-2.69359277789063,-2.69305187597094,-2.69228507760071,
-2.69182724913245),.UNSPECIFIED.);
#224=B_SPLINE_CURVE_WITH_KNOTS('',3,(#39231,#39232,#39233,#39234,#39235,
#39236,#39237,#39238,#39239,#39240,#39241,#39242,#39243,#39244,#39245,#39246,
#39247,#39248,#39249,#39250,#39251,#39252,#39253,#39254,#39255,#39256,#39257,
#39258,#39259,#39260,#39261,#39262,#39263,#39264,#39265,#39266,#39267,#39268,
#39269,#39270,#39271,#39272,#39273,#39274,#39275,#39276,#39277,#39278,#39279,
#39280,#39281,#39282,#39283,#39284,#39285,#39286,#39287,#39288,#39289,#39290,
#39291,#39292,#39293,#39294,#39295,#39296,#39297,#39298,#39299,#39300,#39301,
#39302,#39303,#39304,#39305,#39306,#39307,#39308,#39309,#39310,#39311,#39312,
#39313,#39314,#39315,#39316,#39317,#39318,#39319,#39320,#39321,#39322,#39323,
#39324,#39325,#39326,#39327,#39328,#39329,#39330,#39331,#39332,#39333,#39334,
#39335,#39336,#39337,#39338,#39339,#39340,#39341,#39342,#39343,#39344,#39345,
#39346,#39347,#39348,#39349,#39350,#39351,#39352,#39353,#39354,#39355,#39356,
#39357,#39358,#39359,#39360,#39361,#39362,#39363,#39364,#39365,#39366,#39367,
#39368,#39369,#39370,#39371,#39372,#39373,#39374,#39375,#39376,#39377,#39378,
#39379,#39380,#39381,#39382,#39383,#39384,#39385,#39386,#39387,#39388,#39389,
#39390,#39391,#39392,#39393,#39394,#39395,#39396,#39397,#39398,#39399,#39400,
#39401,#39402,#39403,#39404,#39405,#39406,#39407,#39408,#39409,#39410,#39411,
#39412,#39413,#39414,#39415,#39416,#39417,#39418,#39419,#39420,#39421,#39422,
#39423,#39424,#39425,#39426,#39427,#39428,#39429,#39430,#39431,#39432,#39433,
#39434,#39435,#39436,#39437,#39438,#39439,#39440),.UNSPECIFIED.,.F.,.F.,
(4,2,2,2,2,2,2,2,2,2,2,2,2,2,2,2,2,2,2,2,2,2,2,2,2,2,2,2,2,2,2,2,2,2,2,
2,2,2,2,2,2,2,2,2,2,2,2,2,2,2,2,2,2,2,2,2,2,2,2,2,2,2,2,2,2,2,2,2,2,2,2,
2,2,2,2,2,2,2,2,2,2,2,2,2,2,2,2,2,2,2,2,2,2,2,2,2,2,2,2,2,2,2,2,2,4),(-1.37031440543437,
-1.34985354582264,-1.3438291591212,-1.34196249922411,-1.34094886086762,
-1.33994426827501,-1.33874711848388,-1.33652773334125,-1.33376719865848,
-1.28542360784259,-1.19094435320615,-1.18958082640232,-1.18800304602631,
-1.18534912746519,-1.18097453191006,-1.17983734857757,-1.17918177336801,
-1.17862147635709,-1.17793579652214,-1.17662820256177,-1.16876650062564,
-1.1540884961261,-1.14096899212298,-1.03960529394694,-1.03548316042706,
-1.03341370898517,-1.03259656691607,-1.03076767472717,-1.0268368247659,
-1.02072296182719,-1.01884541548855,-1.01782956487744,-1.01682510437983,
-1.01563126972847,-1.01343137992386,-1.01069800495569,-1.00491525643778,
-0.989074744870986,-0.958690409897572,-0.862853286709799,-0.85794230843511,
-0.856861347755493,-0.856161534428666,-0.855600350758997,-0.854955677235901,
-0.85383694889709,-0.849175704344511,-0.82672368350558,-0.814053521446936,
-0.73031131485283,-0.699755447923921,-0.696925857829539,-0.695561004061509,
-0.694592504495004,-0.693618888355921,-0.692346674735723,-0.689777192123046,
-0.686472387413955,-0.679005711864414,-0.656773472916899,-0.621359921809086,
-0.544497083646594,-0.543626192470129,-0.541439523851208,-0.541133172326015,
-0.535116267439142,-0.533955068482497,-0.533230540814627,-0.532666907973655,
-0.53203794461443,-0.53098960464022,-0.527135506865875,-0.438542204284299,
-0.406785890764745,-0.376732074824184,-0.373914056312083,-0.372552022913521,
-0.371584275156491,-0.370611178305843,-0.36962843616908,-0.367483554618584,
-0.357080181678513,-0.337311734680935,-0.313369220878766,-0.216672402140462,
-0.211855842791534,-0.210782373639322,-0.210084841892462,-0.20952375867137,
-0.208877269918677,-0.20775060802432,-0.202989665487318,-0.160059907314356,
-0.0970476351608282,-0.0912954534780944,-0.0755067392938426,-0.0533397442101704,
-0.0507380336612936,-0.0494298080432169,-0.0484762518739942,-0.0475127683795713,
-0.0465193091884311,-0.0452243237816687,-0.0431876943653371,-0.000960726247794841),
 .UNSPECIFIED.);
#225=B_SPLINE_CURVE_WITH_KNOTS('',3,(#39441,#39442,#39443,#39444,#39445,
#39446,#39447,#39448,#39449,#39450,#39451,#39452,#39453,#39454,#39455,#39456,
#39457,#39458,#39459,#39460,#39461,#39462,#39463,#39464,#39465,#39466,#39467,
#39468,#39469,#39470,#39471,#39472,#39473,#39474,#39475,#39476,#39477,#39478,
#39479,#39480,#39481,#39482,#39483,#39484,#39485,#39486,#39487,#39488,#39489,
#39490,#39491,#39492,#39493,#39494,#39495,#39496,#39497,#39498,#39499,#39500,
#39501,#39502,#39503,#39504,#39505,#39506,#39507,#39508,#39509,#39510,#39511,
#39512,#39513,#39514,#39515,#39516,#39517,#39518,#39519,#39520,#39521,#39522,
#39523,#39524,#39525,#39526,#39527,#39528,#39529,#39530,#39531,#39532,#39533,
#39534,#39535,#39536,#39537,#39538,#39539,#39540,#39541,#39542,#39543,#39544,
#39545,#39546,#39547,#39548,#39549,#39550,#39551,#39552),.UNSPECIFIED.,
 .F.,.F.,(4,2,2,2,2,2,2,2,2,2,2,2,2,2,2,2,2,2,2,2,2,2,2,2,2,2,2,2,2,2,2,
2,2,2,2,2,2,2,2,2,2,2,2,2,2,2,2,2,2,2,2,2,2,2,2,4),(-4.06033398351104,-3.99325575896065,
-3.96396145968547,-3.95370949610167,-3.94830325600619,-3.94713020088203,
-3.94647370673597,-3.94596984710917,-3.94539724101121,-3.94431608714047,
-3.94060237696248,-3.93972944119854,-3.83744482629944,-3.8179274018609,
-3.79121622778603,-3.78734223937179,-3.78618092764658,-3.78522774447348,
-3.7843235507462,-3.78316526685376,-3.7812052663126,-3.77415490574808,-3.7705556292229,
-3.7690612398609,-3.76852616508363,-3.76713549856036,-3.76652172219038,
-3.76444091178738,-3.76293807605746,-3.76173350473988,-3.76034818210871,
-3.75414547491261,-3.74649070751717,-3.71764773498423,-3.628871923601,-3.62638330375413,
-3.6245544633291,-3.62376823392448,-3.62319542396173,-3.62266567489052,
-3.62194024562897,-3.62012493316739,-3.61641298369729,-3.53035523667217,
-3.49938106983598,-3.47718630595116,-3.46972951891099,-3.4664282436174,
-3.46386466595557,-3.46259203876634,-3.4616191592552,-3.4606515175096,-3.45928887386699,
-3.4564671156655,-3.42621010760946,-3.39966259726345),.UNSPECIFIED.);
#226=B_SPLINE_CURVE_WITH_KNOTS('',3,(#39553,#39554,#39555,#39556,#39557,
#39558,#39559,#39560,#39561,#39562,#39563,#39564,#39565,#39566,#39567,#39568,
#39569,#39570,#39571,#39572,#39573,#39574,#39575,#39576,#39577,#39578,#39579,
#39580,#39581,#39582,#39583,#39584,#39585,#39586,#39587,#39588,#39589,#39590,
#39591,#39592,#39593,#39594,#39595,#39596,#39597,#39598,#39599,#39600,#39601,
#39602,#39603,#39604,#39605,#39606,#39607,#39608,#39609,#39610,#39611,#39612,
#39613,#39614,#39615,#39616,#39617,#39618,#39619,#39620,#39621,#39622,#39623,
#39624,#39625,#39626,#39627,#39628,#39629,#39630,#39631,#39632,#39633,#39634,
#39635,#39636,#39637,#39638,#39639,#39640,#39641,#39642,#39643,#39644,#39645,
#39646,#39647,#39648,#39649,#39650,#39651,#39652,#39653,#39654,#39655,#39656,
#39657,#39658,#39659,#39660,#39661,#39662,#39663,#39664,#39665,#39666,#39667,
#39668,#39669,#39670,#39671,#39672,#39673,#39674,#39675,#39676,#39677,#39678,
#39679,#39680,#39681,#39682,#39683,#39684,#39685,#39686,#39687,#39688,#39689,
#39690,#39691,#39692,#39693,#39694,#39695,#39696,#39697,#39698,#39699,#39700,
#39701,#39702,#39703,#39704,#39705,#39706,#39707,#39708,#39709,#39710,#39711,
#39712,#39713,#39714,#39715,#39716,#39717,#39718,#39719,#39720,#39721,#39722,
#39723,#39724,#39725,#39726,#39727,#39728,#39729,#39730,#39731,#39732,#39733,
#39734,#39735,#39736,#39737,#39738,#39739,#39740,#39741,#39742,#39743,#39744,
#39745,#39746,#39747,#39748,#39749,#39750,#39751,#39752,#39753,#39754,#39755,
#39756,#39757,#39758,#39759,#39760,#39761,#39762,#39763,#39764,#39765,#39766,
#39767,#39768,#39769,#39770,#39771,#39772,#39773,#39774,#39775,#39776,#39777,
#39778,#39779,#39780,#39781,#39782,#39783,#39784,#39785,#39786,#39787,#39788,
#39789,#39790,#39791,#39792,#39793,#39794,#39795,#39796,#39797,#39798,#39799,
#39800,#39801,#39802,#39803,#39804,#39805,#39806,#39807,#39808,#39809,#39810,
#39811,#39812),.UNSPECIFIED.,.F.,.F.,(4,2,2,2,2,2,2,2,2,2,2,2,2,2,2,2,2,
2,2,2,2,2,2,2,2,2,2,2,2,2,2,2,2,2,2,2,2,2,2,2,2,2,2,2,2,2,2,2,2,2,2,2,2,
2,2,2,2,2,2,2,2,2,2,2,2,2,2,2,2,2,2,2,2,2,2,2,2,2,2,2,2,2,2,2,2,2,2,2,2,
2,2,2,2,2,2,2,2,2,2,2,2,2,2,2,2,2,2,2,2,2,2,2,2,2,2,2,2,2,2,2,2,2,2,2,2,
2,2,2,2,4),(-2.69182724913245,-2.69021737643475,-2.65825795739905,-2.58460862661745,
-2.5513781104368,-2.53654745415856,-2.53417896831157,-2.53293286373868,
-2.53202255858695,-2.5310455713401,-2.52964951869221,-2.52581178359971,
-2.46691997400996,-2.43153893675863,-2.37467763143315,-2.37233389942129,
-2.37145652546998,-2.37086544010598,-2.37029203612731,-2.36960073746184,
-2.3678748722168,-2.35205643839174,-2.25827162252114,-2.23179160703465,
-2.21375645601447,-2.21126584275741,-2.21000449770419,-2.20909223143685,
-2.20812175254827,-2.20647051929564,-2.20201530441772,-2.1326794421864,
-2.08667222427382,-2.07343427550269,-2.05292010699533,-2.04962053808891,
-2.04862944571759,-2.04801338910414,-2.04744645650479,-2.04670938370279,
-2.04510591528097,-2.03300961099021,-2.03099285405789,-2.00468313915824,
-1.89580293195177,-1.88965815615834,-1.887777118519,-1.8867606914821,-1.88575648341966,
-1.88453956264867,-1.88226008588713,-1.8695389105778,-1.844744687504,-1.75519720363045,
-1.72812297591816,-1.72619548948106,-1.72545091285084,-1.72491605790831,
-1.72434642649189,-1.72357925631012,-1.72185733255494,-1.6765735312575,
-1.57285830927401,-1.5666330997393,-1.56474248673439,-1.56372414675436,
-1.5627297013904,-1.56154438010085,-1.55937933600542,-1.55670073861329,
-1.50534955500438,-1.40863938801605,-1.40382981982381,-1.40275715439446,
-1.40205999887493,-1.40149911974161,-1.40085275541368,-1.39972603475847,
-1.39496095513637,-1.35185545785978,-1.24975298892972,-1.24354362058159,
-1.24165484025532,-1.24063684132499,-1.23964232899484,-1.23845653272119,
-1.23629636849744,-1.23362041078573,-1.18249410735551,-1.08552437079673,
-1.08073283531703,-1.079661584516,-1.0789648530639,-1.07840398075966,-1.07775725014604,
-1.0766289597187,-1.07184405632949,-1.01702452278643,-0.940451079906658,
-0.939255584957217,-0.936220686212519,-0.934619133470207,-0.933976813784099,
-0.931943668374321,-0.929789509926258,-0.921025844263873,-0.919090103766099,
-0.917834448831157,-0.916827531551712,-0.915710145911843,-0.913963815691909,
-0.911821803790093,-0.907667747491708,-0.897515209060679,-0.862092713898233,
-0.767623998352655,-0.76627917751271,-0.764704803620338,-0.762086748279053,
-0.761612423217398,-0.757606402994916,-0.756506206240144,-0.755859241638221,
-0.755298313520025,-0.754601701909895,-0.753241932916879,-0.744076720849981,
-0.721632892976202,-0.680949136162185,-0.661764158671516),.UNSPECIFIED.);
#227=B_SPLINE_CURVE_WITH_KNOTS('',3,(#39817,#39818,#39819,#39820,#39821,
#39822,#39823,#39824,#39825,#39826,#39827,#39828,#39829,#39830,#39831,#39832,
#39833,#39834,#39835,#39836,#39837,#39838,#39839,#39840,#39841,#39842,#39843,
#39844,#39845,#39846,#39847,#39848,#39849,#39850,#39851,#39852,#39853,#39854,
#39855,#39856,#39857,#39858,#39859,#39860,#39861,#39862,#39863,#39864,#39865,
#39866,#39867,#39868,#39869,#39870,#39871,#39872,#39873,#39874,#39875,#39876,
#39877,#39878,#39879,#39880,#39881,#39882,#39883,#39884,#39885,#39886,#39887,
#39888,#39889,#39890,#39891,#39892,#39893,#39894,#39895,#39896,#39897,#39898,
#39899,#39900,#39901,#39902,#39903,#39904,#39905,#39906,#39907,#39908,#39909,
#39910,#39911,#39912,#39913,#39914,#39915,#39916,#39917,#39918,#39919,#39920,
#39921,#39922,#39923,#39924,#39925,#39926,#39927,#39928,#39929,#39930,#39931,
#39932,#39933,#39934,#39935,#39936,#39937,#39938,#39939,#39940,#39941,#39942,
#39943,#39944,#39945,#39946,#39947,#39948,#39949,#39950,#39951,#39952,#39953,
#39954,#39955,#39956,#39957,#39958,#39959,#39960,#39961,#39962,#39963,#39964,
#39965,#39966,#39967,#39968,#39969,#39970,#39971,#39972,#39973,#39974,#39975,
#39976,#39977,#39978,#39979,#39980,#39981,#39982,#39983,#39984,#39985,#39986,
#39987,#39988,#39989,#39990,#39991,#39992,#39993,#39994,#39995,#39996,#39997,
#39998,#39999,#40000,#40001,#40002,#40003,#40004,#40005,#40006,#40007,#40008,
#40009,#40010,#40011,#40012,#40013,#40014,#40015,#40016,#40017,#40018,#40019,
#40020,#40021,#40022,#40023,#40024,#40025,#40026,#40027,#40028,#40029,#40030,
#40031,#40032,#40033,#40034,#40035,#40036,#40037,#40038,#40039,#40040,#40041,
#40042,#40043,#40044,#40045,#40046,#40047,#40048,#40049,#40050,#40051,#40052,
#40053,#40054,#40055,#40056,#40057,#40058,#40059,#40060,#40061,#40062,#40063,
#40064,#40065,#40066,#40067,#40068,#40069,#40070,#40071,#40072,#40073,#40074,
#40075,#40076,#40077,#40078),.UNSPECIFIED.,.F.,.F.,(4,2,2,2,2,2,2,2,2,2,
2,2,2,2,2,2,2,2,2,2,2,2,2,2,2,2,2,2,2,2,2,2,2,2,2,2,2,2,2,2,2,2,2,2,2,2,
2,2,2,2,2,2,2,2,2,2,2,2,2,2,2,2,2,2,2,2,2,2,2,2,2,2,2,2,2,2,2,2,2,2,2,2,
2,2,2,2,2,2,2,2,2,2,2,2,2,2,2,2,2,2,2,2,2,2,2,2,2,2,2,2,2,2,2,2,2,2,2,2,
2,2,2,2,2,2,2,2,2,2,2,2,4),(-3.40032058230379,-3.3799374648879,-3.34212549608457,
-3.28371974346358,-3.28073584446632,-3.27937774803398,-3.27835761528463,
-3.27740085619244,-3.27607968493925,-3.27270795511768,-3.22697058758892,
-3.15481958391072,-3.14172149518491,-3.12656532004299,-3.12178848192617,
-3.11976092952867,-3.11868003839966,-3.11798199532822,-3.11736468867488,
-3.11681555214059,-3.1162460720554,-3.11518103684641,-3.11161020969522,
-3.11044465586696,-3.00830715877538,-2.97902495345214,-2.95997636602871,
-2.9574547972874,-2.95618713308082,-2.95527400905678,-2.95430606855141,
-2.9529428766579,-2.95011956829779,-2.91981856057307,-2.83266407016917,
-2.81944117769823,-2.79902457581346,-2.79684334916451,-2.79570373891997,
-2.79498104536503,-2.79431129292489,-2.79376200880038,-2.79319442855792,
-2.7921387796893,-2.78864783713265,-2.73263644232016,-2.68233283131275,
-2.65115325770841,-2.63679326515295,-2.6344379654432,-2.63320476495985,
-2.63219948154276,-2.63104290751681,-2.62909155825207,-2.62212785911985,
-2.61799868843131,-2.61678846863385,-2.58912004283622,-2.52818601040035,
-2.47600489618271,-2.47390490216913,-2.47279620947344,-2.47208648515507,
-2.47142644307641,-2.4708774781524,-2.47030379223922,-2.46921788872494,
-2.4654638611272,-2.46464692613671,-2.36205448220919,-2.33345152231888,
-2.31406318767361,-2.31153168751624,-2.31026198281973,-2.30934855518638,
-2.30838137302403,-2.3070210161324,-2.30420931445073,-2.27440655411847,
-2.18680257734629,-2.17357027870461,-2.15309788328493,-2.14980231753782,
-2.14881162771975,-2.14819563541882,-2.14762863130534,-2.14689128659541,
-2.14534427281589,-2.13418932717296,-2.03162347160407,-2.01504796289966,
-2.01252810491902,-1.99149525183495,-1.98868385030345,-1.98735267401199,
-1.98633321310056,-1.98524379103596,-1.98354191542762,-1.97828351202086,
-1.94902102029486,-1.90511091655736,-1.83131928365065,-1.82706733137248,
-1.82594229323562,-1.82528960350133,-1.82472923295969,-1.82404027880153,
-1.82271682839484,-1.81448117532174,-1.79686936304596,-1.77200100434899,
-1.70502744633313,-1.66925042616225,-1.66605040947304,-1.66475857200075,
-1.6638094604679,-1.66280508606322,-1.66146073442565,-1.65996835715344,
-1.65745923748942,-1.59973184090697,-1.50904827671948,-1.50420563682844,
-1.50313018707631,-1.50243210645491,-1.50187107856831,-1.5012252082698,
-1.50010100022417,-1.49536973071829,-1.45335850041969,-1.37031440543437),
 .UNSPECIFIED.);
#228=B_SPLINE_CURVE_WITH_KNOTS('',3,(#40080,#40081,#40082,#40083,#40084,
#40085,#40086,#40087,#40088,#40089,#40090,#40091,#40092,#40093,#40094,#40095,
#40096,#40097,#40098,#40099,#40100,#40101,#40102,#40103,#40104,#40105,#40106,
#40107,#40108,#40109,#40110,#40111,#40112,#40113,#40114,#40115,#40116,#40117,
#40118,#40119,#40120,#40121,#40122,#40123,#40124,#40125,#40126,#40127,#40128,
#40129,#40130,#40131,#40132,#40133,#40134,#40135,#40136,#40137,#40138,#40139,
#40140,#40141,#40142,#40143,#40144,#40145,#40146,#40147,#40148,#40149,#40150,
#40151,#40152,#40153,#40154,#40155,#40156,#40157,#40158,#40159,#40160,#40161,
#40162,#40163,#40164,#40165,#40166,#40167,#40168,#40169,#40170,#40171,#40172,
#40173,#40174,#40175,#40176,#40177,#40178,#40179,#40180,#40181,#40182,#40183,
#40184,#40185),.UNSPECIFIED.,.F.,.F.,(4,2,2,2,2,2,2,2,2,2,2,2,2,2,2,2,2,
2,2,2,2,2,2,2,2,2,2,2,2,2,2,2,2,2,2,2,2,2,2,2,2,2,2,2,2,2,2,2,2,2,2,2,4),
(-0.661764158671516,-0.630026095972386,-0.599660466607192,-0.596835164668896,
-0.595471330715412,-0.594503080907936,-0.593529626220461,-0.592547164926349,
-0.590405266744127,-0.580052738956178,-0.560411913828406,-0.525764839858332,
-0.439582547517306,-0.435716517236515,-0.434138317250194,-0.433378007457329,
-0.432838805051148,-0.432327994870582,-0.431606577921066,-0.430125216079379,
-0.416603358644276,-0.391670308022166,-0.357240898860935,-0.318533321754957,
-0.301470244379321,-0.295599217891707,-0.294040538114015,-0.292806344971613,
-0.291799484974881,-0.275951448748212,-0.27332999752129,-0.272041805663648,
-0.271031222873681,-0.27008822001604,-0.268988646385686,-0.265758570119385,
-0.234624138347925,-0.214725054536103,-0.136351665805889,-0.132958720863464,
-0.128284081036437,-0.125800160660937,-0.124997715274561,-0.123538298531019,
-0.112513858500062,-0.111107523597831,-0.11039017572697,-0.109862278437131,
-0.109287353238062,-0.108491022215696,-0.106605911173784,-0.07180074640157,
-0.000962423497023393),.UNSPECIFIED.);
#229=B_SPLINE_CURVE_WITH_KNOTS('',3,(#40186,#40187,#40188,#40189,#40190,
#40191,#40192,#40193,#40194,#40195,#40196,#40197,#40198,#40199,#40200,#40201,
#40202,#40203,#40204,#40205,#40206,#40207,#40208,#40209,#40210,#40211,#40212,
#40213,#40214,#40215,#40216,#40217,#40218,#40219,#40220,#40221,#40222,#40223,
#40224,#40225,#40226,#40227,#40228,#40229,#40230,#40231,#40232,#40233,#40234,
#40235,#40236,#40237,#40238,#40239,#40240,#40241,#40242,#40243,#40244,#40245,
#40246,#40247,#40248,#40249,#40250,#40251,#40252,#40253,#40254,#40255,#40256,
#40257,#40258,#40259,#40260,#40261,#40262,#40263,#40264,#40265,#40266,#40267,
#40268,#40269,#40270,#40271,#40272,#40273,#40274,#40275,#40276,#40277,#40278,
#40279,#40280,#40281,#40282,#40283,#40284,#40285,#40286,#40287,#40288,#40289,
#40290,#40291,#40292,#40293,#40294,#40295,#40296,#40297,#40298,#40299,#40300,
#40301,#40302,#40303,#40304,#40305,#40306,#40307,#40308,#40309,#40310,#40311,
#40312,#40313,#40314,#40315,#40316,#40317,#40318,#40319,#40320,#40321,#40322,
#40323,#40324,#40325,#40326,#40327,#40328,#40329,#40330,#40331,#40332,#40333,
#40334,#40335,#40336,#40337,#40338,#40339,#40340,#40341,#40342,#40343,#40344,
#40345,#40346,#40347,#40348,#40349,#40350,#40351,#40352,#40353,#40354,#40355,
#40356,#40357,#40358,#40359,#40360,#40361,#40362,#40363,#40364,#40365,#40366,
#40367,#40368,#40369,#40370,#40371,#40372,#40373,#40374,#40375,#40376,#40377,
#40378,#40379,#40380,#40381,#40382,#40383,#40384,#40385,#40386,#40387,#40388,
#40389,#40390,#40391,#40392,#40393,#40394,#40395,#40396,#40397,#40398,#40399,
#40400,#40401,#40402,#40403,#40404,#40405,#40406,#40407,#40408,#40409,#40410,
#40411,#40412,#40413,#40414,#40415,#40416,#40417,#40418,#40419,#40420,#40421),
 .UNSPECIFIED.,.F.,.F.,(4,2,2,2,2,2,2,2,2,2,2,2,2,2,2,2,2,2,2,2,2,2,2,2,
2,2,2,2,2,2,2,2,2,2,2,2,2,2,2,2,2,2,2,2,2,2,2,2,2,2,2,2,2,2,2,2,2,2,2,2,
2,2,2,2,2,2,2,2,2,2,2,2,2,2,2,2,2,2,2,2,2,2,2,2,2,2,2,2,2,2,2,2,2,2,2,2,
2,2,2,2,2,2,2,2,2,2,2,2,2,2,2,2,2,2,2,2,2,4),(-4.06265665564838,-4.01519207432212,
-4.01312846426963,-4.01182202416978,-4.01082448393246,-4.0098637311164,
-4.00891442534306,-4.00762310520072,-4.00442831954379,-3.96896057723717,
-3.96159857501236,-3.95572730743425,-3.87447110344671,-3.85351777991439,
-3.85017457363714,-3.84917829964622,-3.84856084631634,-3.84799390674043,
-3.84725857468516,-3.84603571530434,-3.84154145631612,-3.74737549969145,
-3.71602071727454,-3.69960251958336,-3.69055151222796,-3.68849643895652,
-3.68752229726192,-3.68660861106297,-3.68564020162565,-3.68427655733553,
-3.68145298825952,-3.67386870545059,-3.67205408430674,-3.66999013349106,
-3.66953427855102,-3.66751656089206,-3.6648165736704,-3.66361930774808,
-3.66204427725642,-3.65565080301116,-3.63933102626431,-3.59296419710499,
-3.58744400935408,-3.58103705971439,-3.57343088445997,-3.56401678258572,
-3.52848687925774,-3.52665033373977,-3.52586240098824,-3.52528896068898,
-3.5247590761432,-3.52403411954358,-3.52259811093182,-3.51074294975861,
-3.50996875811447,-3.50953532939472,-3.50859699339859,-3.43816279370622,
-3.40053927180154,-3.38126183450086,-3.37255915196901,-3.36885476382934,
-3.36603541399257,-3.36471280953938,-3.36375216849599,-3.36280302016574,
-3.36151224651823,-3.35832048859493,-3.32299411929447,-3.25034085396535,
-3.20546319800254,-3.20362474100503,-3.20283645387427,-3.20226293217564,
-3.20173310177316,-3.20100840944919,-3.19957349920323,-3.18775142581656,
-3.18695135266194,-3.18656364930523,-3.18556377061379,-3.18435838907648,
-3.18181166115263,-3.18048004752747,-3.12627571859425,-3.07335676548773,
-3.05466697981168,-3.04812455278461,-3.04512857599523,-3.04275761795701,
-3.04152606603022,-3.04061399866939,-3.03964089161196,-3.03826001314669,
-3.03452285622337,-2.97386610832818,-2.9560773992344,-2.91021452722237,
-2.89029214015917,-2.88170964771827,-2.88037158935712,-2.87967934896861,
-2.87917238701352,-2.87862072002632,-2.87764485514921,-2.8747821939702,
-2.82554661290418,-2.76830619470589,-2.74655226678981,-2.72497761090541,
-2.7220572100284,-2.71973327591102,-2.71851277221316,-2.71760218473921,
-2.71662420842439,-2.71522558550321,-2.71137354925264,-2.69339729397568),
 .UNSPECIFIED.);
#230=B_SPLINE_CURVE_WITH_KNOTS('',3,(#40427,#40428,#40429,#40430,#40431,
#40432,#40433,#40434,#40435,#40436,#40437,#40438,#40439,#40440,#40441,#40442,
#40443,#40444,#40445,#40446,#40447,#40448,#40449,#40450,#40451,#40452,#40453,
#40454,#40455,#40456,#40457,#40458,#40459,#40460,#40461,#40462,#40463,#40464,
#40465,#40466,#40467,#40468,#40469,#40470,#40471,#40472,#40473,#40474,#40475,
#40476,#40477,#40478,#40479,#40480,#40481,#40482,#40483,#40484,#40485,#40486,
#40487,#40488,#40489,#40490,#40491,#40492,#40493,#40494,#40495,#40496,#40497,
#40498,#40499,#40500,#40501,#40502,#40503,#40504,#40505,#40506,#40507,#40508,
#40509,#40510,#40511,#40512,#40513,#40514,#40515,#40516,#40517,#40518,#40519,
#40520,#40521,#40522,#40523,#40524,#40525,#40526,#40527,#40528,#40529,#40530,
#40531,#40532,#40533,#40534,#40535,#40536,#40537,#40538,#40539,#40540,#40541,
#40542,#40543,#40544,#40545,#40546,#40547,#40548,#40549,#40550,#40551,#40552,
#40553,#40554,#40555,#40556,#40557,#40558,#40559,#40560,#40561,#40562,#40563,
#40564,#40565,#40566,#40567,#40568,#40569,#40570,#40571,#40572,#40573,#40574,
#40575,#40576,#40577,#40578,#40579,#40580,#40581,#40582,#40583,#40584,#40585,
#40586,#40587,#40588,#40589,#40590,#40591,#40592,#40593,#40594,#40595,#40596,
#40597,#40598,#40599,#40600,#40601,#40602,#40603,#40604,#40605,#40606,#40607,
#40608,#40609,#40610,#40611,#40612,#40613,#40614,#40615,#40616,#40617,#40618,
#40619,#40620,#40621,#40622,#40623,#40624,#40625,#40626,#40627,#40628,#40629,
#40630,#40631,#40632,#40633,#40634,#40635,#40636,#40637,#40638,#40639,#40640,
#40641,#40642,#40643,#40644,#40645,#40646,#40647,#40648,#40649,#40650,#40651,
#40652,#40653,#40654,#40655,#40656,#40657,#40658,#40659,#40660,#40661,#40662,
#40663,#40664),.UNSPECIFIED.,.F.,.F.,(4,2,2,2,2,2,2,2,2,2,2,2,2,2,2,2,2,
2,2,2,2,2,2,2,2,2,2,2,2,2,2,2,2,2,2,2,2,2,2,2,2,2,2,2,2,2,2,2,2,2,2,2,2,
2,2,2,2,2,2,2,2,2,2,2,2,2,2,2,2,2,2,2,2,2,2,2,2,2,2,2,2,2,2,2,2,2,2,2,2,
2,2,2,2,2,2,2,2,2,2,2,2,2,2,2,2,2,2,2,2,2,2,2,2,2,2,2,2,2,4),(-1.3698304902262,
-1.32428933057399,-1.31948879307245,-1.31841674433939,-1.31771971518298,
-1.31717135303647,-1.31654222567829,-1.31547285221714,-1.31417946860804,
-1.31158485767664,-1.2840220018988,-1.16451499058872,-1.15890834890452,
-1.15709434131001,-1.15609137329208,-1.15508576708868,-1.15384555596996,
-1.1514563645641,-1.13626793975227,-1.10172225938852,-1.00079513260847,
-0.998376629750531,-0.99574636522065,-0.994804438739867,-0.994259713517067,
-0.99370580272964,-0.992989698771978,-0.992202556689252,-0.990908733506069,
-0.988312875516995,-0.981635028675933,-0.95563725752181,-0.869883529481548,
-0.862521488314064,-0.857018663457017,-0.855690476526718,-0.854487391421601,
-0.852873042988626,-0.850804291411659,-0.8498630066506,-0.849491825407147,
-0.847431178471495,-0.845617153848005,-0.837977650807255,-0.834888443722276,
-0.833648636533639,-0.832618767657051,-0.831566462010941,-0.830037065949472,
-0.826039354092153,-0.773354181536859,-0.76274030407169,-0.678200182203252,
-0.673237596030051,-0.672152565430984,-0.671451498336876,-0.67092123295971,
-0.670301084612403,-0.669271749185127,-0.668036921857623,-0.665601659217542,
-0.659478618965444,-0.647031632655781,-0.614395319742399,-0.547883827271349,
-0.540079567403126,-0.533987894744303,-0.532580789880052,-0.53136665663084,
-0.530217523221808,-0.514314784954095,-0.511690887189617,-0.510402340048761,
-0.509391868369516,-0.508271178459762,-0.506429917338288,-0.499923277918778,
-0.458617353545733,-0.446872452661901,-0.437624566661491,-0.429964520777408,
-0.423435890055808,-0.417766307164819,-0.412773069448065,-0.366078554089945,
-0.351170915829155,-0.349494262709317,-0.348799838132352,-0.348225596507305,
-0.347699321671372,-0.346892330567366,-0.344930194891345,-0.342189945104828,
-0.335002121289331,-0.310825373154438,-0.260371136784263,-0.216497556505191,
-0.211505644306274,-0.191756062727765,-0.189238465608133,-0.187951828889098,
-0.187003947342121,-0.185977866981315,-0.184584787014969,-0.181410256467709,
-0.139156688342432,-0.0509635004110096,-0.0473269913994285,-0.0443169920642124,
-0.0417706281933888,-0.02815904282542,-0.0266665397668058,-0.0259274181360774,
-0.0253939015293733,-0.0248569146346794,-0.0243003809023242,-0.0235698893386271,
-0.0224118256069681,-0.00096066158750924),.UNSPECIFIED.);
#231=B_SPLINE_CURVE_WITH_KNOTS('',3,(#40665,#40666,#40667,#40668,#40669,
#40670,#40671,#40672,#40673,#40674,#40675,#40676,#40677,#40678,#40679,#40680,
#40681,#40682,#40683,#40684,#40685,#40686,#40687,#40688,#40689,#40690,#40691,
#40692,#40693,#40694,#40695,#40696,#40697,#40698,#40699,#40700,#40701,#40702,
#40703,#40704,#40705,#40706,#40707,#40708,#40709,#40710,#40711,#40712,#40713,
#40714,#40715,#40716,#40717,#40718,#40719,#40720,#40721,#40722,#40723,#40724,
#40725,#40726,#40727,#40728,#40729,#40730,#40731,#40732,#40733,#40734,#40735,
#40736,#40737,#40738,#40739,#40740,#40741,#40742,#40743,#40744,#40745,#40746,
#40747,#40748,#40749,#40750,#40751,#40752,#40753,#40754,#40755,#40756,#40757,
#40758,#40759,#40760,#40761,#40762),.UNSPECIFIED.,.F.,.F.,(4,2,2,2,2,2,
2,2,2,2,2,2,2,2,2,2,2,2,2,2,2,2,2,2,2,2,2,2,2,2,2,2,2,2,2,2,2,2,2,2,2,2,
2,2,2,2,2,2,4),(-4.06158090041823,-3.96121984395872,-3.94175624083592,-3.92850692032922,
-3.92620208661939,-3.92497983597762,-3.92397549030708,-3.92296254403926,
-3.92109844107742,-3.91509238718933,-3.79931151758472,-3.78072060932732,
-3.77030457747063,-3.76670833095255,-3.76506418274644,-3.76376375652012,
-3.76308350811494,-3.76252493050456,-3.76187714026647,-3.76077308870359,
-3.75672863766171,-3.75630672469111,-3.75368472373727,-3.75211090308495,
-3.7186870091084,-3.69906245647009,-3.6615266660199,-3.62218340155293,-3.60572584072176,
-3.60328849763299,-3.60203816178099,-3.6011273659431,-3.60015231899455,
-3.59876317750513,-3.59497005068115,-3.53315354605583,-3.47742059325199,
-3.4643646876459,-3.45012892852547,-3.44492118037184,-3.44276017708284,
-3.44162825491389,-3.44066874520663,-3.44006500874364,-3.43949809933791,
-3.43876121291962,-3.43715876353481,-3.42508993849536,-3.40032058230379),
 .UNSPECIFIED.);
#232=B_SPLINE_CURVE_WITH_KNOTS('',3,(#40763,#40764,#40765,#40766,#40767,
#40768,#40769,#40770,#40771,#40772,#40773,#40774,#40775,#40776,#40777,#40778,
#40779,#40780,#40781,#40782,#40783,#40784,#40785,#40786,#40787,#40788,#40789,
#40790,#40791,#40792,#40793,#40794,#40795,#40796,#40797,#40798,#40799,#40800,
#40801,#40802,#40803,#40804,#40805,#40806,#40807,#40808,#40809,#40810,#40811,
#40812,#40813,#40814,#40815,#40816,#40817,#40818,#40819,#40820,#40821,#40822,
#40823,#40824,#40825,#40826,#40827,#40828,#40829,#40830,#40831,#40832,#40833,
#40834,#40835,#40836,#40837,#40838,#40839,#40840,#40841,#40842,#40843,#40844,
#40845,#40846,#40847,#40848,#40849,#40850,#40851,#40852,#40853,#40854,#40855,
#40856,#40857,#40858,#40859,#40860,#40861,#40862,#40863,#40864,#40865,#40866,
#40867,#40868,#40869,#40870,#40871,#40872,#40873,#40874,#40875,#40876,#40877,
#40878,#40879,#40880,#40881,#40882,#40883,#40884,#40885,#40886,#40887,#40888,
#40889,#40890,#40891,#40892,#40893,#40894,#40895,#40896,#40897,#40898,#40899,
#40900,#40901,#40902,#40903,#40904,#40905,#40906,#40907,#40908,#40909,#40910,
#40911,#40912,#40913,#40914,#40915,#40916,#40917,#40918,#40919,#40920,#40921,
#40922,#40923,#40924,#40925,#40926,#40927,#40928,#40929,#40930,#40931,#40932,
#40933,#40934,#40935,#40936,#40937,#40938,#40939,#40940,#40941,#40942,#40943,
#40944,#40945,#40946,#40947,#40948,#40949,#40950,#40951,#40952,#40953,#40954,
#40955,#40956,#40957,#40958,#40959,#40960,#40961,#40962,#40963,#40964,#40965,
#40966,#40967,#40968,#40969,#40970,#40971,#40972,#40973,#40974,#40975,#40976,
#40977,#40978,#40979,#40980,#40981,#40982,#40983,#40984,#40985,#40986,#40987,
#40988,#40989,#40990,#40991,#40992,#40993,#40994,#40995,#40996,#40997,#40998,
#40999,#41000,#41001,#41002,#41003,#41004,#41005,#41006,#41007,#41008,#41009,
#41010,#41011,#41012,#41013,#41014,#41015,#41016,#41017,#41018,#41019,#41020,
#41021,#41022,#41023,#41024,#41025,#41026,#41027,#41028,#41029,#41030,#41031,
#41032,#41033,#41034,#41035,#41036,#41037,#41038,#41039,#41040,#41041,#41042,
#41043,#41044,#41045,#41046,#41047,#41048,#41049,#41050,#41051,#41052,#41053,
#41054,#41055,#41056,#41057,#41058),.UNSPECIFIED.,.F.,.F.,(4,2,2,2,2,2,
2,2,2,2,2,2,2,2,2,2,2,2,2,2,2,2,2,2,2,2,2,2,2,2,2,2,2,2,2,2,2,2,2,2,2,2,
2,2,2,2,2,2,2,2,2,2,2,2,2,2,2,2,2,2,2,2,2,2,2,2,2,2,2,2,2,2,2,2,2,2,2,2,
2,2,2,2,2,2,2,2,2,2,2,2,2,2,2,2,2,2,2,2,2,2,2,2,2,2,2,2,2,2,2,2,2,2,2,2,
2,2,2,2,2,2,2,2,2,2,2,2,2,2,2,2,2,2,2,2,2,2,2,2,2,2,2,2,2,2,2,2,2,4),(-2.69339729397568,
-2.65070256896701,-2.56185162080011,-2.55807568284471,-2.55703458106043,
-2.55640704715056,-2.55584276078045,-2.5551147496108,-2.55360096451557,
-2.54369393474394,-2.54119861290314,-2.53936703346992,-2.44851580038719,
-2.42584793755402,-2.40210297604234,-2.39901597915292,-2.39658428836075,
-2.39534086308734,-2.39442706667613,-2.39345864486377,-2.39209515421873,
-2.38927245944913,-2.38168588342074,-2.37987037215632,-2.37780613827738,
-2.37735648789383,-2.37649300859573,-2.37442117695808,-2.37282220936172,
-2.37161790754733,-2.37030672687911,-2.36235115980645,-2.33342087300233,
-2.31416461982431,-2.27869168641303,-2.25063483858677,-2.24057872494133,
-2.23524708131059,-2.23407845254968,-2.23342259462732,-2.23291834450145,
-2.23234435389043,-2.23125780484793,-2.22750093263263,-2.16716361119526,
-2.1183454568295,-2.08100995136657,-2.07488664936594,-2.07308485763927,
-2.07197270132617,-2.07095969105062,-2.06965359577783,-2.06694310145696,
-2.04923703472158,-2.04477511220494,-2.03186986825692,-1.98640636545065,
-1.91635069540718,-1.9121484407553,-1.91102789463409,-1.91037599913304,
-1.90981518559431,-1.90912426906663,-1.9077927286498,-1.89937547193282,
-1.88034893507459,-1.85494792524301,-1.77779876797247,-1.77405237696026,
-1.75357098639904,-1.75074352732453,-1.74942894204689,-1.74841158346819,
-1.74731393013775,-1.74557713694573,-1.74003359769068,-1.70820883303056,
-1.66242401709319,-1.59300021985711,-1.58903215274263,-1.58793558484484,
-1.58728927389974,-1.58673904526217,-1.58608698590166,-1.58536324197837,
-1.58422148544993,-1.58203512981867,-1.56154817337327,-1.54089963874239,
-1.43501694765643,-1.42878156302234,-1.42688894239053,-1.4258697553289,
-1.42487462764692,-1.42366435536843,-1.42141816436874,-1.40936838489987,
-1.38559989939009,-1.34014581549528,-1.27589427376871,-1.27453722731701,
-1.27295923601943,-1.27031187285776,-1.26592902817596,-1.26479078675474,
-1.26413482703853,-1.26358537257141,-1.26291828704283,-1.26219941874474,
-1.26106920273423,-1.25891313556766,-1.20527170670429,-1.11115614921505,
-1.10552052161462,-1.10370220460565,-1.10269804146774,-1.10169200819346,
-1.10045241260208,-1.09806796051367,-1.08302059758581,-1.04902629263222,
-0.94726209072256,-0.946065598114438,-0.942512328583506,-0.941448974233042,
-0.940879632521123,-0.94037299481827,-0.939723257934841,-0.93856497078791,
-0.937137595362479,-0.934170310341013,-0.926161130851365,-0.900140778734837,
-0.809725910550172,-0.803510070067896,-0.80203686444722,-0.800827345210138,
-0.799526136163081,-0.78369314250953,-0.78107207453701,-0.77978380027982,
-0.778773028119492,-0.777651475659123,-0.775807586722291,-0.769279502083752,
-0.727753271970297,-0.68465412528036,-0.662515798853911),.UNSPECIFIED.);
#233=B_SPLINE_CURVE_WITH_KNOTS('',3,(#41063,#41064,#41065,#41066,#41067,
#41068,#41069,#41070,#41071,#41072,#41073,#41074,#41075,#41076,#41077,#41078,
#41079,#41080,#41081,#41082,#41083,#41084,#41085,#41086,#41087,#41088,#41089,
#41090,#41091,#41092,#41093,#41094,#41095,#41096,#41097,#41098,#41099,#41100,
#41101,#41102,#41103,#41104,#41105,#41106,#41107,#41108,#41109,#41110,#41111,
#41112,#41113,#41114,#41115,#41116,#41117,#41118,#41119,#41120,#41121,#41122,
#41123,#41124,#41125,#41126,#41127,#41128,#41129,#41130,#41131,#41132,#41133,
#41134,#41135,#41136,#41137,#41138,#41139,#41140,#41141,#41142,#41143,#41144,
#41145,#41146,#41147,#41148,#41149,#41150,#41151,#41152,#41153,#41154,#41155,
#41156,#41157,#41158,#41159,#41160,#41161,#41162,#41163,#41164,#41165,#41166,
#41167,#41168,#41169,#41170,#41171,#41172,#41173,#41174,#41175,#41176,#41177,
#41178,#41179,#41180,#41181,#41182,#41183,#41184,#41185,#41186,#41187,#41188,
#41189,#41190,#41191,#41192,#41193,#41194,#41195,#41196,#41197,#41198,#41199,
#41200,#41201,#41202,#41203,#41204,#41205,#41206,#41207,#41208,#41209,#41210,
#41211,#41212,#41213,#41214,#41215,#41216,#41217,#41218,#41219,#41220,#41221,
#41222,#41223,#41224,#41225,#41226,#41227,#41228,#41229,#41230,#41231,#41232,
#41233,#41234,#41235,#41236,#41237,#41238,#41239,#41240,#41241,#41242,#41243,
#41244,#41245,#41246,#41247,#41248,#41249,#41250,#41251,#41252,#41253,#41254,
#41255,#41256,#41257,#41258,#41259,#41260,#41261,#41262,#41263,#41264,#41265,
#41266,#41267,#41268,#41269,#41270,#41271,#41272,#41273,#41274,#41275,#41276,
#41277,#41278,#41279,#41280,#41281,#41282,#41283,#41284,#41285,#41286,#41287,
#41288,#41289,#41290,#41291,#41292,#41293,#41294,#41295,#41296,#41297,#41298,
#41299,#41300,#41301,#41302,#41303,#41304,#41305,#41306,#41307,#41308,#41309,
#41310,#41311,#41312,#41313,#41314),.UNSPECIFIED.,.F.,.F.,(4,2,2,2,2,2,
2,2,2,2,2,2,2,2,2,2,2,2,2,2,2,2,2,2,2,2,2,2,2,2,2,2,2,2,2,2,2,2,2,2,2,2,
2,2,2,2,2,2,2,2,2,2,2,2,2,2,2,2,2,2,2,2,2,2,2,2,2,2,2,2,2,2,2,2,2,2,2,2,
2,2,2,2,2,2,2,2,2,2,2,2,2,2,2,2,2,2,2,2,2,2,2,2,2,2,2,2,2,2,2,2,2,2,2,2,
2,2,2,2,2,2,2,2,2,2,2,4),(-3.40051625466855,-3.38690541455584,-3.29044724348338,
-3.26182515764191,-3.25917667588228,-3.25725462489775,-3.25645194662039,
-3.25587582132367,-3.25534925660727,-3.25463722419276,-3.25325163385757,
-3.2427742022924,-3.14888251686569,-3.1259149138765,-3.10185442059904,-3.09719754494597,
-3.09557286172972,-3.09463097013533,-3.0936578702247,-3.09240296646104,
-3.08995249069854,-3.07631855204624,-3.0759108883163,-3.06280325578392,
-2.9944847485952,-2.9396157336949,-2.93482999960508,-2.93370135045011,-2.93305438698172,
-2.93249329577895,-2.93179627242911,-2.9307245383389,-2.92593024470862,
-2.83839821057211,-2.77826275267882,-2.77398055322274,-2.77240850017005,
-2.77146704313098,-2.77046947700221,-2.76916901166849,-2.76650486519096,
-2.76340131264863,-2.68466730315942,-2.63581402890625,-2.61638155158392,
-2.61169127291663,-2.61057010115868,-2.60992480882675,-2.60936356912183,
-2.60866430825142,-2.60758535187923,-2.60270114104014,-2.50661658037635,
-2.47325099501405,-2.45267365450566,-2.45010863753982,-2.44884889051031,
-2.44787079423109,-2.44678664156047,-2.44507940440876,-2.44000822910834,
-2.35754081200886,-2.33411547965245,-2.30175434425609,-2.29327589962243,
-2.28857373653641,-2.28745166784889,-2.28680619727978,-2.28624500924613,
-2.28554607851144,-2.28446812165807,-2.27959593184768,-2.18513398554553,
-2.13165235681725,-2.12763911299052,-2.12610717286206,-2.12505420270318,
-2.12402453156198,-2.12278598363417,-2.1197052715485,-2.09153095940257,
-2.06180893345821,-2.03079833106906,-1.9788587385233,-1.97780567351586,
-1.96630110262639,-1.96472011759108,-1.96398719463192,-1.96342079068491,
-1.96280255116963,-1.96180209855782,-1.95841829966425,-1.93704358169982,
-1.91325698683968,-1.81122573363896,-1.80528287711341,-1.80342611911971,
-1.80241441768905,-1.801409562889,-1.80018416514624,-1.79786580618383,-1.78433969447462,
-1.76281990219557,-1.71774508637011,-1.64652664800121,-1.64247609741258,
-1.6413712992311,-1.64072326773154,-1.6401735004104,-1.63949812202562,-1.63876695437737,
-1.63760719800645,-1.63537281832261,-1.61410789402183,-1.59053766742233,
-1.48825184801937,-1.4822503421835,-1.48038647250649,-1.47937339283081,
-1.47836874925764,-1.47714589771116,-1.47483921777996,-1.46156089437542,
-1.44368541513119,-1.41935152810288,-1.3698304902262),.UNSPECIFIED.);
#234=B_SPLINE_CURVE_WITH_KNOTS('',3,(#41316,#41317,#41318,#41319,#41320,
#41321,#41322,#41323,#41324,#41325,#41326,#41327,#41328,#41329,#41330,#41331,
#41332,#41333,#41334,#41335,#41336,#41337,#41338,#41339,#41340,#41341,#41342,
#41343,#41344,#41345,#41346,#41347,#41348,#41349,#41350,#41351,#41352,#41353,
#41354,#41355,#41356,#41357,#41358,#41359,#41360,#41361,#41362,#41363,#41364,
#41365,#41366,#41367,#41368,#41369,#41370,#41371,#41372,#41373,#41374,#41375,
#41376,#41377,#41378,#41379,#41380,#41381,#41382,#41383,#41384,#41385,#41386,
#41387,#41388,#41389,#41390,#41391,#41392,#41393,#41394,#41395,#41396,#41397,
#41398,#41399,#41400,#41401,#41402,#41403,#41404,#41405,#41406,#41407,#41408,
#41409,#41410,#41411,#41412,#41413,#41414,#41415),.UNSPECIFIED.,.F.,.F.,
(4,2,2,2,2,2,2,2,2,2,2,2,2,2,2,2,2,2,2,2,2,2,2,2,2,2,2,2,2,2,2,2,2,2,2,
2,2,2,2,2,2,2,2,2,2,2,2,2,2,4),(-0.662515798853911,-0.622949123215544,-0.619410428437198,
-0.618348821592143,-0.617779855577449,-0.61727348175795,-0.61662335073915,
-0.615461241975333,-0.614029492323155,-0.611049758161222,-0.602994553941927,
-0.582591376448421,-0.464885700533223,-0.459078084680766,-0.457237914063416,
-0.456229405836154,-0.455324525615237,-0.454136371618478,-0.451991683794027,
-0.441691859967688,-0.422235387403578,-0.369406626324371,-0.346797847004858,
-0.315359670773203,-0.31176284413968,-0.311165310532351,-0.309750598088807,
-0.308997290185044,-0.297114933102574,-0.295519246214448,-0.294783510064955,
-0.294216647726752,-0.293691522326338,-0.292801384326984,-0.290312890080721,
-0.28660728759925,-0.275758530936159,-0.256353821445812,-0.177202364163881,
-0.161461846237226,-0.15888819944909,-0.137860606717043,-0.135012274995971,
-0.133694002962819,-0.132676353075674,-0.131580919887413,-0.129852994620517,
-0.124381467664199,-0.0326164518727757,-0.000962543441835597),
 .UNSPECIFIED.);
#235=B_SPLINE_CURVE_WITH_KNOTS('',3,(#41416,#41417,#41418,#41419,#41420,
#41421,#41422,#41423,#41424,#41425,#41426,#41427,#41428,#41429,#41430,#41431,
#41432,#41433,#41434,#41435,#41436,#41437,#41438,#41439,#41440,#41441,#41442,
#41443,#41444,#41445,#41446,#41447,#41448,#41449,#41450,#41451,#41452,#41453,
#41454,#41455,#41456,#41457,#41458,#41459,#41460,#41461,#41462,#41463,#41464,
#41465,#41466,#41467,#41468,#41469,#41470,#41471,#41472,#41473,#41474,#41475,
#41476,#41477,#41478,#41479,#41480,#41481,#41482,#41483,#41484,#41485,#41486,
#41487,#41488,#41489,#41490,#41491,#41492,#41493,#41494,#41495,#41496,#41497,
#41498,#41499,#41500,#41501,#41502,#41503,#41504,#41505,#41506,#41507,#41508,
#41509,#41510,#41511,#41512,#41513,#41514,#41515,#41516,#41517,#41518,#41519,
#41520,#41521,#41522,#41523,#41524,#41525,#41526,#41527,#41528,#41529,#41530,
#41531,#41532,#41533,#41534,#41535,#41536,#41537,#41538,#41539,#41540,#41541,
#41542,#41543,#41544,#41545,#41546,#41547,#41548,#41549,#41550,#41551,#41552,
#41553,#41554,#41555,#41556,#41557,#41558,#41559,#41560,#41561,#41562,#41563,
#41564,#41565,#41566,#41567,#41568,#41569,#41570,#41571,#41572,#41573,#41574,
#41575,#41576,#41577,#41578,#41579,#41580,#41581,#41582,#41583,#41584,#41585,
#41586,#41587,#41588,#41589,#41590,#41591,#41592,#41593,#41594,#41595,#41596,
#41597,#41598,#41599,#41600,#41601,#41602,#41603,#41604,#41605,#41606,#41607,
#41608,#41609,#41610,#41611,#41612,#41613,#41614,#41615,#41616,#41617,#41618,
#41619,#41620,#41621,#41622,#41623,#41624,#41625,#41626,#41627,#41628,#41629,
#41630,#41631,#41632,#41633,#41634,#41635,#41636,#41637,#41638,#41639,#41640,
#41641,#41642,#41643,#41644,#41645,#41646,#41647,#41648,#41649,#41650,#41651,
#41652,#41653,#41654,#41655,#41656,#41657,#41658,#41659,#41660,#41661,#41662,
#41663,#41664,#41665),.UNSPECIFIED.,.F.,.F.,(4,2,2,2,2,2,2,2,2,2,2,2,2,
2,2,2,2,2,2,2,2,2,2,2,2,2,2,2,2,2,2,2,2,2,2,2,2,2,2,2,2,2,2,2,2,2,2,2,2,
2,2,2,2,2,2,2,2,2,2,2,2,2,2,2,2,2,2,2,2,2,2,2,2,2,2,2,2,2,2,2,2,2,2,2,2,
2,2,2,2,2,2,2,2,2,2,2,2,2,2,2,2,2,2,2,2,2,2,2,2,2,2,2,2,2,2,2,2,2,2,2,2,
2,2,2,4),(-4.0596306034683,-4.03408001543506,-4.03284230580221,-4.03170089899201,
-4.03097756808815,-4.03042373629631,-4.02988513142353,-4.02934905080663,
-4.02859941912943,-4.02706360203124,-4.01191427368421,-4.01088880758094,
-4.00695556671887,-4.00259288122757,-3.99879678480457,-3.92038330815872,
-3.88759839889834,-3.87286396112631,-3.87049385401555,-3.86925792642461,
-3.86834927503052,-3.86736850537898,-3.86595760047595,-3.86201915130986,
-3.79801492584274,-3.74918338795194,-3.72749401875158,-3.71549138511218,
-3.71150146194004,-3.70886194487888,-3.70795327373198,-3.70742801778671,
-3.70686347063613,-3.706141292649,-3.70461486335358,-3.69439946013216,-3.6922147214184,
-3.69124229647514,-3.68257061893155,-3.63689995490928,-3.63161815457147,
-3.62553548874142,-3.61841228804763,-3.60985877235864,-3.59913723358057,
-3.56525610322083,-3.55024196353418,-3.54786034373455,-3.54662196201688,
-3.54561678399208,-3.5446133657065,-3.54279609643532,-3.53716148935955,
-3.44334607352452,-3.41156627664411,-3.39501784720514,-3.38962202868366,
-3.38740390849395,-3.38625045409914,-3.38527079066045,-3.38466502365465,
-3.38409903877816,-3.38336721957741,-3.38179077893482,-3.37038791533419,
-3.36830240252975,-3.36680624056531,-3.28754070723922,-3.24331774492344,
-3.22744220416606,-3.22502692419042,-3.22378145826932,-3.22278492279516,
-3.22164145714426,-3.21969672018744,-3.2129999374358,-3.20920949631288,
-3.20516314771942,-3.20475690458286,-3.20267336689837,-3.20146592327029,
-3.20025443429063,-3.19873737695966,-3.19251620843431,-3.10217498483601,
-3.07620828638405,-3.06816710065458,-3.06519197002561,-3.06376218451645,
-3.06260272101135,-3.06195296993781,-3.06144715052437,-3.06079310040788,
-3.05966177859417,-3.05534404352915,-2.95177595452284,-2.91911179588142,
-2.90440680881616,-2.9020377769674,-2.90080201522956,-2.89979698349377,
-2.89879206137503,-2.89696744076646,-2.89127597270991,-2.88911797889175,
-2.88479916972265,-2.88410396155892,-2.88257827035607,-2.88049092384788,
-2.87865122004206,-2.87742741771214,-2.87593728901736,-2.86991356312346,
-2.86204544015667,-2.82739388957354,-2.74398120228353,-2.74169769204191,
-2.74051959611997,-2.73978085024382,-2.73911187661108,-2.73856146983336,
-2.73800409849907,-2.73699845355724,-2.73390788155705,-2.69171368309219),
 .UNSPECIFIED.);
#236=B_SPLINE_CURVE_WITH_KNOTS('',3,(#41671,#41672,#41673,#41674,#41675,
#41676,#41677,#41678,#41679,#41680,#41681,#41682,#41683,#41684,#41685,#41686,
#41687,#41688,#41689,#41690,#41691,#41692,#41693,#41694,#41695,#41696,#41697,
#41698,#41699,#41700,#41701,#41702,#41703,#41704,#41705,#41706,#41707,#41708,
#41709,#41710,#41711,#41712,#41713,#41714,#41715,#41716,#41717,#41718,#41719,
#41720,#41721,#41722,#41723,#41724,#41725,#41726,#41727,#41728,#41729,#41730,
#41731,#41732,#41733,#41734,#41735,#41736,#41737,#41738,#41739,#41740,#41741,
#41742,#41743,#41744,#41745,#41746,#41747,#41748,#41749,#41750,#41751,#41752,
#41753,#41754,#41755,#41756,#41757,#41758,#41759,#41760,#41761,#41762,#41763,
#41764,#41765,#41766,#41767,#41768,#41769,#41770,#41771,#41772,#41773,#41774,
#41775,#41776,#41777,#41778,#41779,#41780,#41781,#41782,#41783,#41784,#41785,
#41786,#41787,#41788,#41789,#41790,#41791,#41792,#41793,#41794,#41795,#41796,
#41797,#41798,#41799,#41800,#41801,#41802,#41803,#41804,#41805,#41806,#41807,
#41808,#41809,#41810,#41811,#41812,#41813,#41814,#41815,#41816,#41817,#41818,
#41819,#41820,#41821,#41822,#41823,#41824,#41825,#41826,#41827,#41828,#41829,
#41830,#41831,#41832,#41833,#41834,#41835,#41836,#41837,#41838,#41839,#41840,
#41841,#41842,#41843,#41844,#41845,#41846,#41847,#41848,#41849,#41850,#41851,
#41852,#41853,#41854,#41855,#41856,#41857,#41858,#41859,#41860,#41861,#41862,
#41863,#41864,#41865,#41866,#41867,#41868,#41869,#41870,#41871,#41872,#41873,
#41874,#41875,#41876,#41877,#41878),.UNSPECIFIED.,.F.,.F.,(4,2,2,2,2,2,
2,2,2,2,2,2,2,2,2,2,2,2,2,2,2,2,2,2,2,2,2,2,2,2,2,2,2,2,2,2,2,2,2,2,2,2,
2,2,2,2,2,2,2,2,2,2,2,2,2,2,2,2,2,2,2,2,2,2,2,2,2,2,2,2,2,2,2,2,2,2,2,2,
2,2,2,2,2,2,2,2,2,2,2,2,2,2,2,2,2,2,2,2,2,2,2,2,2,4),(-1.36987613430623,
-1.30423436574626,-1.29811626324107,-1.29627565662543,-1.29513741718348,
-1.29415021048094,-1.29292585758167,-1.29160164608747,-1.28551314135413,
-1.22912540670448,-1.1514675610177,-1.15039164910677,-1.14999982222173,
-1.14917565738476,-1.14856659640192,-1.14757758861731,-1.13599509150043,
-1.13456888154719,-1.1338465289113,-1.1333174206724,-1.13274368225986,-1.13195336291943,
-1.13010235918765,-1.07879156098914,-1.01183753385623,-0.977350897628902,
-0.974177654777872,-0.972890327588509,-0.971942249931243,-0.970936837811205,
-0.969587134846786,-0.96808762884725,-0.958704957096693,-0.941527649371185,
-0.920577195061325,-0.86947729467201,-0.828095524617837,-0.825345004238373,
-0.822496376121744,-0.820889035414862,-0.819416935803335,-0.816869616095077,
-0.815885577195018,-0.812241128523552,-0.811167542563649,-0.810596304375256,
-0.810041485613778,-0.809361030782193,-0.808078076187776,-0.800752014359733,
-0.785412099906747,-0.767208555586726,-0.755505275941498,-0.745623005829675,
-0.684287783424875,-0.654336071043674,-0.651269518831263,-0.650000965646211,
-0.649057624431322,-0.648048804984938,-0.646677074345568,-0.645148759473659,
-0.635073861785818,-0.616181333057069,-0.592577846690027,-0.506035342388049,
-0.490351704678072,-0.488629633387516,-0.487938871576626,-0.487365525035434,
-0.486774079505288,-0.48589541586769,-0.483487625313566,-0.444383945728644,
-0.421291102608374,-0.390511981655186,-0.332109263843609,-0.328527432577969,
-0.327171470527913,-0.326205262954542,-0.32520973250963,-0.32391924591181,
-0.322503597214568,-0.314871297805738,-0.237897467758746,-0.179515446691896,
-0.17767097291996,-0.167086050594585,-0.16569637141602,-0.164983313387578,
-0.164456516221019,-0.163880677574938,-0.163079355626802,-0.161165052577766,
-0.158530029303512,-0.130180035919145,-0.0517939334688018,-0.0100431515482136,
-0.00573742005696059,-0.00410925369192486,-0.00314308150865512,-0.00217102557994161,
-0.00115611315314765,-0.000961498652879823),.UNSPECIFIED.);
#237=B_SPLINE_CURVE_WITH_KNOTS('',3,(#41879,#41880,#41881,#41882,#41883,
#41884,#41885,#41886,#41887,#41888,#41889,#41890,#41891,#41892,#41893,#41894,
#41895,#41896,#41897,#41898,#41899,#41900,#41901,#41902,#41903,#41904,#41905,
#41906,#41907,#41908,#41909,#41910,#41911,#41912,#41913,#41914,#41915,#41916,
#41917,#41918,#41919,#41920,#41921,#41922,#41923,#41924,#41925,#41926,#41927,
#41928,#41929,#41930,#41931,#41932,#41933,#41934,#41935,#41936,#41937,#41938,
#41939,#41940,#41941,#41942,#41943,#41944,#41945,#41946,#41947,#41948,#41949,
#41950,#41951,#41952,#41953,#41954,#41955,#41956,#41957,#41958,#41959,#41960,
#41961,#41962,#41963,#41964,#41965,#41966,#41967,#41968,#41969,#41970,#41971,
#41972),.UNSPECIFIED.,.F.,.F.,(4,2,2,2,2,2,2,2,2,2,2,2,2,2,2,2,2,2,2,2,
2,2,2,2,2,2,2,2,2,2,2,2,2,2,2,2,2,2,2,2,2,2,2,2,2,2,4),(-4.06152144056539,
-4.06068140455345,-4.05639989610793,-3.99939524463301,-3.93815796338596,
-3.91398161098074,-3.90439152400712,-3.90301674327762,-3.90231701789723,
-3.90176099769942,-3.90120101898099,-3.90018324148975,-3.89700056397345,
-3.84186610269507,-3.79113917844855,-3.76884803001755,-3.74759770649987,
-3.74328295757049,-3.74170635388609,-3.74076506738686,-3.7397684490541,
-3.73847187051845,-3.73582568920672,-3.71833684272978,-3.62662415397337,
-3.58209910484305,-3.58026263986025,-3.57947481607542,-3.57890148332518,
-3.57837171917564,-3.57764695854626,-3.57621143270756,-3.56436424142731,
-3.5642206697547,-3.56283798950838,-3.5614878900379,-3.55907159397315,-3.51970491019132,
-3.46869822090784,-3.42394639885459,-3.42010894945472,-3.41860420573156,
-3.41766132551795,-3.41665409833314,-3.41529737921832,-3.41235685579398,
-3.40051625466855),.UNSPECIFIED.);
#238=B_SPLINE_CURVE_WITH_KNOTS('',3,(#41973,#41974,#41975,#41976,#41977,
#41978,#41979,#41980,#41981,#41982,#41983,#41984,#41985,#41986,#41987,#41988,
#41989,#41990,#41991,#41992,#41993,#41994,#41995,#41996,#41997,#41998,#41999,
#42000,#42001,#42002,#42003,#42004,#42005,#42006,#42007,#42008,#42009,#42010,
#42011,#42012,#42013,#42014,#42015,#42016,#42017,#42018,#42019,#42020,#42021,
#42022,#42023,#42024,#42025,#42026,#42027,#42028,#42029,#42030,#42031,#42032,
#42033,#42034,#42035,#42036,#42037,#42038,#42039,#42040,#42041,#42042,#42043,
#42044,#42045,#42046,#42047,#42048,#42049,#42050,#42051,#42052,#42053,#42054,
#42055,#42056,#42057,#42058,#42059,#42060,#42061,#42062,#42063,#42064,#42065,
#42066,#42067,#42068,#42069,#42070,#42071,#42072,#42073,#42074,#42075,#42076,
#42077,#42078,#42079,#42080,#42081,#42082,#42083,#42084,#42085,#42086,#42087,
#42088,#42089,#42090,#42091,#42092,#42093,#42094,#42095,#42096,#42097,#42098,
#42099,#42100,#42101,#42102,#42103,#42104,#42105,#42106,#42107,#42108,#42109,
#42110,#42111,#42112,#42113,#42114,#42115,#42116,#42117,#42118,#42119,#42120,
#42121,#42122,#42123,#42124,#42125,#42126,#42127,#42128,#42129,#42130,#42131,
#42132,#42133,#42134,#42135,#42136,#42137,#42138,#42139,#42140,#42141,#42142,
#42143,#42144,#42145,#42146,#42147,#42148,#42149,#42150,#42151,#42152,#42153,
#42154,#42155,#42156,#42157,#42158,#42159,#42160,#42161,#42162,#42163,#42164,
#42165,#42166,#42167,#42168,#42169,#42170,#42171,#42172,#42173,#42174,#42175,
#42176,#42177,#42178,#42179,#42180,#42181,#42182,#42183,#42184,#42185,#42186,
#42187,#42188,#42189,#42190,#42191,#42192,#42193,#42194,#42195,#42196,#42197,
#42198,#42199,#42200,#42201,#42202,#42203,#42204,#42205,#42206,#42207,#42208,
#42209,#42210,#42211,#42212,#42213,#42214,#42215,#42216,#42217,#42218,#42219,
#42220,#42221,#42222,#42223,#42224,#42225,#42226,#42227,#42228,#42229,#42230,
#42231,#42232,#42233,#42234,#42235,#42236,#42237,#42238,#42239,#42240,#42241,
#42242,#42243,#42244,#42245,#42246,#42247,#42248,#42249,#42250,#42251,#42252,
#42253,#42254,#42255,#42256,#42257,#42258),.UNSPECIFIED.,.F.,.F.,(4,2,2,
2,2,2,2,2,2,2,2,2,2,2,2,2,2,2,2,2,2,2,2,2,2,2,2,2,2,2,2,2,2,2,2,2,2,2,2,
2,2,2,2,2,2,2,2,2,2,2,2,2,2,2,2,2,2,2,2,2,2,2,2,2,2,2,2,2,2,2,2,2,2,2,2,
2,2,2,2,2,2,2,2,2,2,2,2,2,2,2,2,2,2,2,2,2,2,2,2,2,2,2,2,2,2,2,2,2,2,2,2,
2,2,2,2,2,2,2,2,2,2,2,2,2,2,2,2,2,2,2,2,2,2,2,2,2,2,2,2,2,2,2,4),(-2.69171368309219,
-2.6834459837058,-2.62982931510195,-2.60083134579719,-2.58189109315544,
-2.57937317708939,-2.57810643031875,-2.57719360280117,-2.5762256382986,
-2.57486185784924,-2.57203552430532,-2.54158207936534,-2.454598442427,-2.44138213204764,
-2.4209882973397,-2.41880871173648,-2.41766979496211,-2.41670601595081,
-2.41610116601716,-2.41553478118276,-2.41480076821842,-2.41321311081192,
-2.40152586189933,-2.35729451210967,-2.33133511868389,-2.3037434151305,
-2.27880070171448,-2.25914273988751,-2.25660374311802,-2.25533258187017,
-2.25441901382055,-2.2534525218016,-2.25209450490336,-2.24929207125282,
-2.24168527229027,-2.23979352264476,-2.2387547465452,-2.23833373698779,
-2.23706899470299,-2.23497867901234,-2.23268535126204,-2.23148756544026,
-2.22987949183382,-2.22349992178107,-2.14631344688755,-2.12141405431791,
-2.103777826941,-2.0955399947309,-2.09421653519785,-2.09352761440454,-2.09296729079571,
-2.09240005695671,-2.09134588304041,-2.08786663208743,-2.03131222958311,
-1.94041243609069,-1.9349097120671,-1.93310937127585,-1.93210921061048,
-1.93111289840147,-1.92987223042552,-1.92748056084247,-1.91222587243804,
-1.87742633311048,-1.78406204017884,-1.77292496318781,-1.77137877748411,
-1.77064164004646,-1.77007471007355,-1.76945870983849,-1.76846782122739,
-1.76516993242197,-1.7446757700911,-1.73145330775892,-1.64370152734678,
-1.61413261114428,-1.61132657432292,-1.60996765292093,-1.60900090085964,
-1.60800709318742,-1.60672037194052,-1.60530979442929,-1.60299736826935,
-1.59838630961833,-1.55115064625895,-1.45409036483056,-1.44924778746479,
-1.4481025931723,-1.44744519233895,-1.44689039812731,-1.44620942153864,
-1.444923850799,-1.4375413673796,-1.42208245677764,-1.40892146603893,-1.32515132758051,
-1.29127709173573,-1.2881181894425,-1.28683348005702,-1.28588616742654,
-1.28488042266633,-1.28352630486411,-1.28202242438181,-1.27948550867864,
-1.20143317623793,-1.13856807004486,-1.12697225249683,-1.12554567628525,
-1.12482326565083,-1.12429417622832,-1.1237205199338,-1.12293042043797,
-1.12108041317263,-1.07111078932753,-1.0129160316982,-0.9686256971168,-0.965274849938421,
-0.963957142455952,-0.963001250848394,-0.962002107085687,-0.960680606096423,
-0.959221909953988,-0.956794172854803,-0.951868502983901,-0.860647303969667,
-0.822429623753632,-0.820723462521068,-0.818454479535298,-0.817277380238017,
-0.816400074058821,-0.814712279699945,-0.803955067175405,-0.802558983640366,
-0.801844346802657,-0.801317216677441,-0.800741869241858,-0.799942738954365,
-0.798040720255703,-0.795426806270093,-0.767488954905554,-0.716580306283524,
-0.686214775624197,-0.662215315077933),.UNSPECIFIED.);
#239=B_SPLINE_CURVE_WITH_KNOTS('',3,(#42263,#42264,#42265,#42266,#42267,
#42268,#42269,#42270,#42271,#42272,#42273,#42274,#42275,#42276,#42277,#42278,
#42279,#42280,#42281,#42282,#42283,#42284,#42285,#42286,#42287,#42288,#42289,
#42290,#42291,#42292,#42293,#42294,#42295,#42296,#42297,#42298,#42299,#42300,
#42301,#42302,#42303,#42304,#42305,#42306,#42307,#42308,#42309,#42310,#42311,
#42312,#42313,#42314,#42315,#42316,#42317,#42318,#42319,#42320,#42321,#42322,
#42323,#42324,#42325,#42326,#42327,#42328,#42329,#42330,#42331,#42332,#42333,
#42334,#42335,#42336,#42337,#42338,#42339,#42340,#42341,#42342,#42343,#42344,
#42345,#42346,#42347,#42348,#42349,#42350,#42351,#42352,#42353,#42354,#42355,
#42356,#42357,#42358,#42359,#42360,#42361,#42362,#42363,#42364,#42365,#42366,
#42367,#42368,#42369,#42370,#42371,#42372,#42373,#42374,#42375,#42376,#42377,
#42378,#42379,#42380,#42381,#42382,#42383,#42384,#42385,#42386,#42387,#42388,
#42389,#42390,#42391,#42392,#42393,#42394,#42395,#42396,#42397,#42398,#42399,
#42400,#42401,#42402,#42403,#42404,#42405,#42406,#42407,#42408,#42409,#42410,
#42411,#42412,#42413,#42414,#42415,#42416,#42417,#42418,#42419,#42420,#42421,
#42422,#42423,#42424,#42425,#42426,#42427,#42428,#42429,#42430,#42431,#42432,
#42433,#42434,#42435,#42436,#42437,#42438,#42439,#42440,#42441,#42442,#42443,
#42444,#42445,#42446,#42447,#42448,#42449,#42450,#42451,#42452,#42453,#42454,
#42455,#42456,#42457,#42458,#42459,#42460,#42461,#42462,#42463,#42464,#42465,
#42466,#42467,#42468,#42469,#42470,#42471,#42472,#42473,#42474,#42475,#42476,
#42477,#42478,#42479,#42480,#42481,#42482,#42483,#42484,#42485,#42486,#42487,
#42488,#42489,#42490,#42491,#42492,#42493,#42494,#42495,#42496,#42497,#42498,
#42499,#42500,#42501,#42502,#42503,#42504,#42505,#42506,#42507,#42508,#42509,
#42510,#42511,#42512,#42513,#42514,#42515,#42516,#42517,#42518,#42519,#42520,
#42521,#42522,#42523,#42524,#42525,#42526,#42527,#42528,#42529,#42530,#42531,
#42532,#42533,#42534,#42535,#42536,#42537,#42538,#42539,#42540,#42541,#42542,
#42543,#42544,#42545,#42546,#42547,#42548,#42549,#42550,#42551,#42552,#42553,
#42554,#42555,#42556,#42557,#42558,#42559,#42560,#42561,#42562,#42563,#42564,
#42565,#42566,#42567,#42568,#42569,#42570,#42571,#42572,#42573,#42574),
 .UNSPECIFIED.,.F.,.F.,(4,2,2,2,2,2,2,2,2,2,2,2,2,2,2,2,2,2,2,2,2,2,2,2,
2,2,2,2,2,2,2,2,2,2,2,2,2,2,2,2,2,2,2,2,2,2,2,2,2,2,2,2,2,2,2,2,2,2,2,2,
2,2,2,2,2,2,2,2,2,2,2,2,2,2,2,2,2,2,2,2,2,2,2,2,2,2,2,2,2,2,2,2,2,2,2,2,
2,2,2,2,2,2,2,2,2,2,2,2,2,2,2,2,2,2,2,2,2,2,2,2,2,2,2,2,2,2,2,2,2,2,2,2,
2,2,2,2,2,2,2,2,2,2,2,2,2,2,2,2,2,2,2,2,2,2,2,4),(-3.39995023952435,-3.39790066675237,
-3.39647554338721,-3.39531839591686,-3.39466939020519,-3.3941628559474,
-3.39350747895038,-3.39237083965205,-3.38800052013932,-3.30986736661366,
-3.29781501467423,-3.28589623440827,-3.25653148664586,-3.23745178257696,
-3.23492925938281,-3.23366138561753,-3.23274821767803,-3.23178032992174,
-3.23041737502309,-3.22759508668623,-3.22001540203264,-3.21820233110779,
-3.2161395714001,-3.21567962739949,-3.21482505227885,-3.21275437897285,
-3.21115770714825,-3.20995415177942,-3.20864383704753,-3.20247849077143,
-3.11188475322385,-3.08566910456112,-3.07783672016234,-3.07491821067812,
-3.07350834455919,-3.07267325509279,-3.07194060851529,-3.0713794764826,
-3.07084909896983,-3.07012169343935,-3.06829568553229,-3.0468612763854,
-2.97110392994944,-2.91666198446861,-2.91263174144541,-2.91109740062427,
-2.9100440823094,-2.90901508542667,-2.90777856998407,-2.90470928590416,
-2.89704322219085,-2.8952264563716,-2.89316585723297,-2.89279820480907,
-2.89185203346652,-2.88978292200772,-2.8881673481913,-2.88696397865985,
-2.88563624672462,-2.88010094240642,-2.86297139255846,-2.78642153828411,
-2.77330338809929,-2.75347857185489,-2.75133473475138,-2.75020931701263,
-2.74949256999691,-2.7488274144646,-2.74827825173216,-2.74770796380214,
-2.74663894992142,-2.74303386040555,-2.6853016252567,-2.63817349918101,
-2.59689095850564,-2.59038589670011,-2.58854486466318,-2.58742426732301,
-2.58641384871073,-2.58512532742226,-2.58250133730334,-2.56659436911881,
-2.5654522657683,-2.5642375553304,-2.56258903137233,-2.55631849527417,-2.47888185542894,
-2.43052788453324,-2.4283984213266,-2.42727845525793,-2.42656397839662,
-2.42590048476646,-2.42534242960493,-2.42476832422689,-2.42368047003734,
-2.41990938144759,-2.35831457109675,-2.33530954161544,-2.31072021846032,
-2.26971802830651,-2.26649592541021,-2.26509431412158,-2.26406670460222,
-2.26312074881111,-2.26184179621844,-2.25871643895931,-2.22632332949083,
-2.14107475443467,-2.12155743592282,-2.10992376517262,-2.10469937808016,
-2.10353846530059,-2.10288442504077,-2.10238036608172,-2.10180529809044,
-2.10071285584473,-2.09690098697674,-2.03157418266106,-1.94931965694971,
-1.94419670464287,-1.9424475215289,-1.94145739602333,-1.94055004817484,
-1.93933081508783,-1.93704185324756,-1.92414092186055,-1.89947793153787,
-1.80970500212944,-1.7828437948926,-1.78091909972448,-1.7801748175239,-1.77963990868748,
-1.77906996196085,-1.77830193509584,-1.77657629368887,-1.72982597768656,
-1.627302407254,-1.62125144730327,-1.61941870818423,-1.61828230243568,-1.61729473534568,
-1.61606910124171,-1.6147415703603,-1.60860350461782,-1.57110518123865,
-1.49079653385519,-1.45978295883548,-1.45779756346203,-1.45704348083467,
-1.45650596722624,-1.45599441638679,-1.45526822408518,-1.45376275383313,
-1.4390395989317,-1.41136436481419,-1.36987613430623),.UNSPECIFIED.);
#240=B_SPLINE_CURVE_WITH_KNOTS('',3,(#42576,#42577,#42578,#42579,#42580,
#42581,#42582,#42583,#42584,#42585,#42586,#42587,#42588,#42589,#42590,#42591,
#42592,#42593,#42594,#42595,#42596,#42597,#42598,#42599,#42600,#42601,#42602,
#42603,#42604,#42605,#42606,#42607,#42608,#42609,#42610,#42611,#42612,#42613,
#42614,#42615,#42616,#42617,#42618,#42619,#42620,#42621,#42622,#42623,#42624,
#42625,#42626,#42627,#42628,#42629,#42630,#42631,#42632,#42633,#42634,#42635,
#42636,#42637,#42638,#42639,#42640,#42641,#42642,#42643,#42644,#42645,#42646,
#42647,#42648,#42649,#42650,#42651,#42652,#42653,#42654,#42655,#42656,#42657,
#42658,#42659,#42660,#42661,#42662,#42663),.UNSPECIFIED.,.F.,.F.,(4,2,2,
2,2,2,2,2,2,2,2,2,2,2,2,2,2,2,2,2,2,2,2,2,2,2,2,2,2,2,2,2,2,2,2,2,2,2,2,
2,2,2,2,4),(-0.662215315077933,-0.645592509828678,-0.642300582460812,-0.640992787899431,
-0.640039418585149,-0.639037417660101,-0.637705679394495,-0.636232911803243,
-0.633771387936118,-0.628752756583026,-0.537544025971857,-0.497362414649182,
-0.495732165966819,-0.494945917470169,-0.481158980150784,-0.479661225169226,
-0.478920780711691,-0.478386904589461,-0.477816371141681,-0.477044709800266,
-0.475298974857173,-0.43425624349702,-0.39102377666103,-0.365785242715528,
-0.322667312670379,-0.319333571761,-0.318018579878763,-0.317063257448861,
-0.316062233502055,-0.314736831577171,-0.31327294134718,-0.310832948545832,
-0.305873943794809,-0.250575977325575,-0.162097704334626,-0.157377156307122,
-0.15631141826443,-0.155616244542065,-0.155111329213675,-0.154482503161208,
-0.153435247639401,-0.149594333680469,-0.0609460746495673,-0.0009618072526365),
 .UNSPECIFIED.);
#241=B_SPLINE_CURVE_WITH_KNOTS('',3,(#42664,#42665,#42666,#42667,#42668,
#42669,#42670,#42671,#42672,#42673,#42674,#42675,#42676,#42677,#42678,#42679,
#42680,#42681,#42682,#42683,#42684,#42685,#42686,#42687,#42688,#42689,#42690,
#42691,#42692,#42693,#42694,#42695,#42696,#42697,#42698,#42699,#42700,#42701,
#42702,#42703,#42704,#42705,#42706,#42707,#42708,#42709,#42710,#42711,#42712,
#42713,#42714,#42715,#42716,#42717,#42718,#42719,#42720,#42721,#42722,#42723,
#42724,#42725,#42726,#42727,#42728,#42729,#42730,#42731,#42732,#42733,#42734,
#42735,#42736,#42737,#42738,#42739,#42740,#42741,#42742,#42743,#42744,#42745,
#42746,#42747,#42748,#42749,#42750,#42751,#42752,#42753,#42754,#42755,#42756,
#42757,#42758,#42759,#42760,#42761,#42762,#42763,#42764,#42765,#42766,#42767,
#42768,#42769,#42770,#42771,#42772,#42773,#42774,#42775,#42776,#42777,#42778,
#42779,#42780,#42781,#42782,#42783,#42784,#42785,#42786,#42787,#42788,#42789,
#42790,#42791,#42792,#42793,#42794,#42795,#42796,#42797,#42798,#42799,#42800,
#42801,#42802,#42803,#42804,#42805,#42806,#42807,#42808,#42809,#42810,#42811,
#42812,#42813,#42814,#42815,#42816,#42817,#42818,#42819,#42820,#42821,#42822,
#42823,#42824,#42825,#42826,#42827,#42828,#42829,#42830,#42831,#42832,#42833,
#42834,#42835,#42836,#42837,#42838,#42839,#42840,#42841,#42842,#42843,#42844,
#42845,#42846,#42847,#42848,#42849),.UNSPECIFIED.,.F.,.F.,(4,2,2,2,2,2,
2,2,2,2,2,2,2,2,2,2,2,2,2,2,2,2,2,2,2,2,2,2,2,2,2,2,2,2,2,2,2,2,2,2,2,2,
2,2,2,2,2,2,2,2,2,2,2,2,2,2,2,2,2,2,2,2,2,2,2,2,2,2,2,2,2,2,2,2,2,2,2,2,
2,2,2,2,2,2,2,2,2,2,2,2,2,2,4),(-4.06324807418118,-4.06094680439846,-4.05858802674299,
-4.05743017218569,-4.05647707394084,-4.05557150509894,-4.05455859235606,
-4.05269756427623,-4.04602351267091,-3.9560165188871,-3.90112033625435,
-3.89633682194676,-3.89520810170527,-3.89456099549257,-3.89399971838414,
-3.89330238398713,-3.89223002456045,-3.88743057944171,-3.79320381259422,
-3.74333625913723,-3.73859711219189,-3.73623708003318,-3.73480629904628,
-3.73350489678219,-3.73250745586161,-3.73154450131164,-3.73020139324132,
-3.72670012948254,-3.66984168053083,-3.64056688350185,-3.63219371423025,
-3.57838329923819,-3.57322085695561,-3.57206404631861,-3.5714107631116,
-3.57090653822118,-3.57033047369,-3.56923372198927,-3.56538483513116,-3.56431884460312,
-3.46653181268291,-3.41988304625247,-3.41529988356628,-3.41299732211902,
-3.41159057004845,-3.41030648973064,-3.40931169938866,-3.40834295326624,
-3.40697809916241,-3.40414963036706,-3.37371225266012,-3.31275956994051,
-3.30288401391805,-3.29122817984202,-3.25194345633793,-3.24953258999275,
-3.24865335104612,-3.24806168285134,-3.24748825129421,-3.24679753825605,
-3.24507637353263,-3.22943568266711,-3.13069947995998,-3.09548497151522,
-3.09158280970419,-3.08953620295569,-3.08823696927282,-3.08703167687051,
-3.08604565638335,-3.08504226193537,-3.08322778285318,-3.07762183505614,
-2.95863497131182,-2.9496534646441,-2.92962944604377,-2.92637728262097,
-2.92539103621352,-2.92477578614392,-2.92420803549647,-2.9234677481213,
-2.92222823477204,-2.91776441721149,-2.82033351201189,-2.77338243199341,
-2.76878373967125,-2.76647540710207,-2.76506621725414,-2.76378032655481,
-2.76278523414449,-2.76181702812809,-2.76017936177847,-2.75581548862038,
-2.69329048899296),.UNSPECIFIED.);
#242=B_SPLINE_CURVE_WITH_KNOTS('',3,(#42855,#42856,#42857,#42858,#42859,
#42860,#42861,#42862,#42863,#42864,#42865,#42866,#42867,#42868,#42869,#42870,
#42871,#42872,#42873,#42874,#42875,#42876,#42877,#42878,#42879,#42880,#42881,
#42882,#42883,#42884,#42885,#42886,#42887,#42888,#42889,#42890,#42891,#42892,
#42893,#42894,#42895,#42896,#42897,#42898,#42899,#42900,#42901,#42902,#42903,
#42904,#42905,#42906,#42907,#42908,#42909,#42910,#42911,#42912,#42913,#42914,
#42915,#42916,#42917,#42918,#42919,#42920,#42921,#42922,#42923,#42924,#42925,
#42926,#42927,#42928,#42929,#42930,#42931,#42932,#42933,#42934,#42935,#42936,
#42937,#42938,#42939,#42940,#42941,#42942,#42943,#42944,#42945,#42946,#42947,
#42948,#42949,#42950,#42951,#42952,#42953,#42954,#42955,#42956,#42957,#42958,
#42959,#42960,#42961,#42962,#42963,#42964,#42965,#42966,#42967,#42968,#42969,
#42970,#42971,#42972,#42973,#42974,#42975,#42976,#42977,#42978,#42979,#42980,
#42981,#42982,#42983,#42984,#42985,#42986,#42987,#42988,#42989,#42990,#42991,
#42992,#42993,#42994,#42995,#42996,#42997,#42998,#42999,#43000,#43001,#43002,
#43003,#43004,#43005,#43006,#43007,#43008,#43009,#43010,#43011,#43012,#43013,
#43014,#43015,#43016,#43017,#43018,#43019,#43020,#43021,#43022,#43023,#43024,
#43025,#43026,#43027,#43028,#43029,#43030,#43031,#43032,#43033,#43034,#43035,
#43036,#43037,#43038,#43039,#43040,#43041,#43042,#43043,#43044,#43045,#43046),
 .UNSPECIFIED.,.F.,.F.,(4,2,2,2,2,2,2,2,2,2,2,2,2,2,2,2,2,2,2,2,2,2,2,2,
2,2,2,2,2,2,2,2,2,2,2,2,2,2,2,2,2,2,2,2,2,2,2,2,2,2,2,2,2,2,2,2,2,2,2,2,
2,2,2,2,2,2,2,2,2,2,2,2,2,2,2,2,2,2,2,2,2,2,2,2,2,2,2,2,2,2,2,2,2,2,2,4),
(-1.37066776653293,-1.33460806111142,-1.27843454625838,-1.27490538137125,
-1.27384494186462,-1.27327623849506,-1.2727443671615,-1.27208334308297,
-1.27137291597215,-1.27026278909526,-1.26815939788736,-1.21596749878615,
-1.15521930543116,-1.13785427222667,-1.13190929371174,-1.12982047984096,
-1.12926390242655,-1.12716725051053,-1.12548600189073,-1.12166452679788,
-1.11501792324622,-1.11307777832825,-1.11193472432678,-1.1109371540384,
-1.10968858488817,-1.1072614968637,-1.0911110942554,-1.05294827720473,-0.962790991629515,
-0.952600010708145,-0.951073492853772,-0.950343005611409,-0.949797106800045,
-0.94918931220958,-0.948213923797306,-0.947058410422206,-0.944835683636722,
-0.939426774461917,-0.922634630263533,-0.898152765055203,-0.826470251911123,
-0.81694246631414,-0.814468380251856,-0.79341426243295,-0.790600678741848,
-0.789268542665083,-0.788248379364131,-0.787158238475457,-0.785455305656051,
-0.780194144236855,-0.75091903178753,-0.696364997018037,-0.649346778261375,
-0.629995686466905,-0.628214493999182,-0.627494609689144,-0.626965990794584,
-0.6264029513512,-0.625632585884956,-0.624769891471457,-0.623292990596328,
-0.620184827786322,-0.61165270590269,-0.590785794557204,-0.474514607689977,
-0.468486227620434,-0.466618637232425,-0.465604561675056,-0.464599578763892,
-0.463377251188843,-0.461074359188197,-0.447889849426173,-0.425643715760829,
-0.37423412107745,-0.350802150871196,-0.310066575548288,-0.305712847800284,
-0.304577554132952,-0.303922336486818,-0.303415819498663,-0.302766161483592,
-0.301605990347403,-0.300177104416431,-0.297205264114373,-0.289178564973308,
-0.268815189127441,-0.151039005620794,-0.145239288404627,-0.143400332558613,
-0.142392196218494,-0.141386955515489,-0.140155348982315,-0.137807807080494,
-0.123630343973804,-0.0933395015526071,-0.000962437203753903),
 .UNSPECIFIED.);
#243=B_SPLINE_CURVE_WITH_KNOTS('',3,(#43047,#43048,#43049,#43050,#43051,
#43052,#43053,#43054,#43055,#43056,#43057,#43058,#43059,#43060,#43061,#43062,
#43063,#43064,#43065,#43066,#43067,#43068,#43069,#43070,#43071,#43072,#43073,
#43074,#43075,#43076,#43077,#43078,#43079,#43080,#43081,#43082,#43083,#43084,
#43085,#43086,#43087,#43088,#43089,#43090,#43091,#43092,#43093,#43094,#43095,
#43096,#43097,#43098,#43099,#43100,#43101,#43102,#43103,#43104,#43105,#43106,
#43107,#43108,#43109,#43110,#43111,#43112,#43113,#43114,#43115,#43116,#43117,
#43118,#43119,#43120,#43121,#43122,#43123,#43124,#43125,#43126,#43127,#43128,
#43129,#43130,#43131,#43132,#43133,#43134,#43135,#43136,#43137,#43138,#43139,
#43140,#43141,#43142,#43143,#43144,#43145,#43146,#43147,#43148,#43149,#43150,
#43151,#43152,#43153,#43154,#43155,#43156,#43157,#43158,#43159,#43160,#43161,
#43162),.UNSPECIFIED.,.F.,.F.,(4,2,2,2,2,2,2,2,2,2,2,2,2,2,2,2,2,2,2,2,
2,2,2,2,2,2,2,2,2,2,2,2,2,2,2,2,2,2,2,2,2,2,2,2,2,2,2,2,2,2,2,2,2,2,2,2,
2,4),(-4.06083114761616,-4.0435233454223,-4.04221098063693,-4.04141623662022,
-4.04083602012308,-4.04031019513466,-4.03973720305329,-4.03904698337022,
-4.03732685989293,-4.02168752395455,-4.01814001032623,-3.91800909934794,
-3.89465292189995,-3.88278521731068,-3.88055013050155,-3.87934287788983,
-3.8784371303106,-3.87729590673197,-3.87536118579213,-3.86875344233555,
-3.86410513177538,-3.86073828272011,-3.86031560717704,-3.85666346852078,
-3.85546887946217,-3.85380973961977,-3.84939833018316,-3.77132316705227,
-3.74620865332801,-3.72801157574431,-3.72252461606231,-3.72027891342914,
-3.71860615325555,-3.71785089510409,-3.71731835358458,-3.71679147311905,
-3.71607711037126,-3.71468137529038,-3.70391995690264,-3.65357828612443,
-3.64839558307956,-3.64251557028934,-3.63574432833506,-3.62778950622246,
-3.61815234105673,-3.60580757540362,-3.5746238042843,-3.5602655900665,-3.55791098872309,
-3.55667819868517,-3.5556732725962,-3.5546665232428,-3.55283313261629,-3.54707368807194,
-3.42900386082964,-3.40885334500813,-3.40086235155439,-3.39995023952435),
 .UNSPECIFIED.);
#244=B_SPLINE_CURVE_WITH_KNOTS('',3,(#43163,#43164,#43165,#43166,#43167,
#43168,#43169,#43170,#43171,#43172,#43173,#43174,#43175,#43176,#43177,#43178,
#43179,#43180,#43181,#43182,#43183,#43184,#43185,#43186,#43187,#43188,#43189,
#43190,#43191,#43192,#43193,#43194,#43195,#43196,#43197,#43198,#43199,#43200,
#43201,#43202,#43203,#43204,#43205,#43206,#43207,#43208,#43209,#43210,#43211,
#43212,#43213,#43214,#43215,#43216,#43217,#43218,#43219,#43220,#43221,#43222,
#43223,#43224,#43225,#43226,#43227,#43228,#43229,#43230,#43231,#43232,#43233,
#43234,#43235,#43236,#43237,#43238,#43239,#43240,#43241,#43242,#43243,#43244,
#43245,#43246,#43247,#43248,#43249,#43250,#43251,#43252,#43253,#43254,#43255,
#43256,#43257,#43258,#43259,#43260,#43261,#43262,#43263,#43264,#43265,#43266,
#43267,#43268,#43269,#43270,#43271,#43272,#43273,#43274,#43275,#43276,#43277,
#43278,#43279,#43280,#43281,#43282,#43283,#43284,#43285,#43286,#43287,#43288,
#43289,#43290,#43291,#43292,#43293,#43294,#43295,#43296,#43297,#43298,#43299,
#43300,#43301,#43302,#43303,#43304,#43305,#43306,#43307,#43308,#43309,#43310,
#43311,#43312,#43313,#43314,#43315,#43316,#43317,#43318,#43319,#43320,#43321,
#43322,#43323,#43324,#43325,#43326,#43327,#43328,#43329,#43330,#43331,#43332,
#43333,#43334,#43335,#43336,#43337,#43338,#43339,#43340,#43341,#43342,#43343,
#43344,#43345,#43346,#43347,#43348,#43349,#43350,#43351,#43352,#43353,#43354,
#43355,#43356,#43357,#43358,#43359,#43360,#43361,#43362,#43363,#43364,#43365,
#43366,#43367,#43368,#43369,#43370,#43371,#43372,#43373,#43374,#43375,#43376,
#43377,#43378,#43379,#43380,#43381,#43382,#43383,#43384,#43385,#43386,#43387,
#43388,#43389,#43390,#43391,#43392,#43393,#43394,#43395,#43396,#43397,#43398,
#43399,#43400,#43401,#43402,#43403,#43404,#43405,#43406,#43407,#43408,#43409,
#43410,#43411,#43412,#43413,#43414,#43415,#43416,#43417,#43418,#43419,#43420,
#43421,#43422,#43423,#43424,#43425,#43426,#43427,#43428,#43429,#43430,#43431,
#43432,#43433,#43434,#43435,#43436,#43437,#43438,#43439,#43440,#43441,#43442,
#43443,#43444,#43445,#43446,#43447,#43448,#43449,#43450,#43451,#43452),
 .UNSPECIFIED.,.F.,.F.,(4,2,2,2,2,2,2,2,2,2,2,2,2,2,2,2,2,2,2,2,2,2,2,2,
2,2,2,2,2,2,2,2,2,2,2,2,2,2,2,2,2,2,2,2,2,2,2,2,2,2,2,2,2,2,2,2,2,2,2,2,
2,2,2,2,2,2,2,2,2,2,2,2,2,2,2,2,2,2,2,2,2,2,2,2,2,2,2,2,2,2,2,2,2,2,2,2,
2,2,2,2,2,2,2,2,2,2,2,2,2,2,2,2,2,2,2,2,2,2,2,2,2,2,2,2,2,2,2,2,2,2,2,2,
2,2,2,2,2,2,2,2,2,2,2,2,4),(-2.69329048899296,-2.68518151524453,-2.63587705543086,
-2.613600490668,-2.60388411526308,-2.60250455754033,-2.60180365388543,-2.60124730553122,
-2.6006047816103,-2.59952435690388,-2.59570739418735,-2.59497548295562,
-2.49206004011417,-2.44971113826612,-2.44536321179857,-2.44314808030844,
-2.44177795228913,-2.44052152797007,-2.43953026098175,-2.43855164307469,
-2.43686092373885,-2.43214789649179,-2.35865987348145,-2.33667142779089,
-2.31482413970386,-2.2935533968185,-2.28500219987506,-2.28027004736997,
-2.27914550992267,-2.27849943023687,-2.27793820750385,-2.27723986834876,
-2.27616399245107,-2.27131899187077,-2.17490631430192,-2.15086749756722,
-2.13422238242691,-2.12082884661321,-2.11851609227305,-2.11729165256605,
-2.11638361779359,-2.1153958713777,-2.11365916027295,-2.10862790806344,
-2.0315412755472,-1.96135779946775,-1.95712473463824,-1.95600121671346,
-1.95534868475304,-1.95478800101291,-1.95409809694128,-1.95277110478572,
-1.94446177464751,-1.92618277154543,-1.9010482540412,-1.82292578135086,
-1.81880679027884,-1.81543657725583,-1.81395000771291,-1.81186558831238,
-1.81127500109984,-1.80963057796859,-1.80876504964641,-1.80285017221233,
-1.79691850516882,-1.79506270729554,-1.79405095953352,-1.79304569682694,
-1.79181927582225,-1.78949739676563,-1.77590849560258,-1.75197219639686,
-1.66214625200846,-1.6353238906885,-1.63339945282677,-1.63265510770978,
-1.63212009858896,-1.63156141219875,-1.63081574006164,-1.62998721837318,
-1.62859364379587,-1.59678532059277,-1.47937774035837,-1.4735561446105,
-1.4717141905978,-1.47070530759669,-1.46980043858811,-1.46861279208966,
-1.46647050711416,-1.45620912691655,-1.43684953741174,-1.41300802459559,
-1.3294468087224,-1.32821474143486,-1.32609752549758,-1.3257023279389,-1.32252085187905,
-1.31145351653741,-1.30990962763432,-1.30917275851862,-1.3086187909282,
-1.30801857257907,-1.30739381187667,-1.30648860949183,-1.30490690183153,
-1.24931038148874,-1.15601490001656,-1.15037992759812,-1.1485617808286,
-1.14755770206493,-1.14655174706372,-1.14531223865232,-1.14292792546519,
-1.12788054567231,-1.0938842988396,-0.992106753281869,-0.991021816513099,
-0.987399600618392,-0.986328310916322,-0.985757398585146,-0.985208084871823,
-0.984589180503195,-0.983891906375962,-0.982813131861444,-0.980791479443496,
-0.976034457111498,-0.96095183161327,-0.947879637922346,-0.881832770804898,
-0.829975828478919,-0.82652672863915,-0.825192294252787,-0.824231715878857,
-0.823212862961879,-0.821865548914382,-0.818941276088402,-0.772217816359426,
-0.759674536721786,-0.748551528660825,-0.669062549622139,-0.667893878600024,
-0.664322310816838,-0.663256833094503,-0.662687068250773,-0.662206116423806),
 .UNSPECIFIED.);
#245=B_SPLINE_CURVE_WITH_KNOTS('',3,(#43457,#43458,#43459,#43460,#43461,
#43462,#43463,#43464,#43465,#43466,#43467,#43468,#43469,#43470,#43471,#43472,
#43473,#43474,#43475,#43476,#43477,#43478,#43479,#43480,#43481,#43482,#43483,
#43484,#43485,#43486,#43487,#43488,#43489,#43490,#43491,#43492,#43493,#43494,
#43495,#43496,#43497,#43498,#43499,#43500,#43501,#43502,#43503,#43504,#43505,
#43506,#43507,#43508,#43509,#43510,#43511,#43512,#43513,#43514,#43515,#43516,
#43517,#43518,#43519,#43520,#43521,#43522,#43523,#43524,#43525,#43526,#43527,
#43528,#43529,#43530,#43531,#43532,#43533,#43534,#43535,#43536,#43537,#43538,
#43539,#43540,#43541,#43542,#43543,#43544,#43545,#43546,#43547,#43548,#43549,
#43550,#43551,#43552,#43553,#43554,#43555,#43556,#43557,#43558,#43559,#43560,
#43561,#43562,#43563,#43564,#43565,#43566,#43567,#43568,#43569,#43570,#43571,
#43572,#43573,#43574,#43575,#43576,#43577,#43578,#43579,#43580,#43581,#43582,
#43583,#43584,#43585,#43586,#43587,#43588,#43589,#43590,#43591,#43592,#43593,
#43594,#43595,#43596,#43597,#43598,#43599,#43600,#43601,#43602,#43603,#43604,
#43605,#43606,#43607,#43608,#43609,#43610,#43611,#43612,#43613,#43614,#43615,
#43616,#43617,#43618,#43619,#43620,#43621,#43622,#43623,#43624,#43625,#43626,
#43627,#43628,#43629,#43630,#43631,#43632,#43633,#43634,#43635,#43636,#43637,
#43638,#43639,#43640,#43641,#43642,#43643,#43644,#43645,#43646,#43647,#43648,
#43649,#43650,#43651,#43652,#43653,#43654,#43655,#43656,#43657,#43658,#43659,
#43660,#43661,#43662,#43663,#43664,#43665,#43666,#43667,#43668,#43669,#43670,
#43671,#43672,#43673,#43674,#43675,#43676,#43677,#43678,#43679,#43680,#43681,
#43682,#43683,#43684,#43685,#43686,#43687,#43688,#43689,#43690,#43691,#43692,
#43693,#43694,#43695,#43696,#43697,#43698,#43699,#43700,#43701,#43702,#43703,
#43704,#43705,#43706,#43707,#43708,#43709,#43710,#43711,#43712,#43713,#43714,
#43715,#43716,#43717,#43718,#43719,#43720,#43721,#43722,#43723,#43724,#43725,
#43726,#43727,#43728,#43729,#43730,#43731,#43732,#43733,#43734,#43735,#43736,
#43737,#43738,#43739,#43740,#43741,#43742,#43743,#43744,#43745,#43746,#43747,
#43748,#43749,#43750,#43751,#43752,#43753,#43754,#43755,#43756,#43757,#43758,
#43759,#43760,#43761,#43762,#43763,#43764,#43765,#43766,#43767,#43768,#43769,
#43770,#43771,#43772,#43773,#43774,#43775,#43776,#43777,#43778),
 .UNSPECIFIED.,.F.,.F.,(4,2,2,2,2,2,2,2,2,2,2,2,2,2,2,2,2,2,2,2,2,2,2,2,
2,2,2,2,2,2,2,2,2,2,2,2,2,2,2,2,2,2,2,2,2,2,2,2,2,2,2,2,2,2,2,2,2,2,2,2,
2,2,2,2,2,2,2,2,2,2,2,2,2,2,2,2,2,2,2,2,2,2,2,2,2,2,2,2,2,2,2,2,2,2,2,2,
2,2,2,2,2,2,2,2,2,2,2,2,2,2,2,2,2,2,2,2,2,2,2,2,2,2,2,2,2,2,2,2,2,2,2,2,
2,2,2,2,2,2,2,2,2,2,2,2,2,2,2,2,2,2,2,2,2,2,2,2,2,2,2,2,4),(-3.40146716175795,
-3.38592178780429,-3.38007580434383,-3.37600311457039,-3.37446646634171,
-3.37352479071898,-3.37250403191549,-3.37116799921537,-3.36892196149448,
-3.35537875389731,-3.35495807869944,-3.3511536937879,-3.34995803509296,
-3.34845852843925,-3.34145898012805,-3.25321113534674,-3.23986682318901,
-3.22229394875692,-3.21405681300377,-3.2127326555314,-3.21204328367722,
-3.2114825480802,-3.21091485883035,-3.20985972982115,-3.20637643641239,
-3.14996442247769,-3.06263767938197,-3.05683586693267,-3.05409536856676,
-3.05189007844652,-3.05069489981988,-3.04968985447596,-3.04867387658602,
-3.04679744857865,-3.04069804112289,-2.93618631090365,-2.89509228270947,
-2.89039017743441,-2.88926780684782,-2.8886221077132,-2.88806068739338,
-2.887361424203,-2.88628287502378,-2.88140679187724,-2.79080447414862,-2.73296079275012,
-2.73046413792708,-2.72897660470029,-2.72763526878433,-2.7266310505314,
-2.72568018745772,-2.72438314297515,-2.7218261917289,-2.70100602609924,
-2.69892741079334,-2.68920742524319,-2.63669427867626,-2.59090078038923,
-2.57512376986321,-2.56753094498153,-2.56623499306395,-2.56555157834579,
-2.56499637896063,-2.56434035788042,-2.56320208178509,-2.55881987950936,
-2.55617163538544,-2.55459409623113,-2.55324070785018,-2.45875739536967,
-2.40973754566531,-2.40727320983504,-2.40579911294765,-2.40446756058742,
-2.403465031549,-2.40251171218893,-2.40120491893475,-2.39792036932,-2.35781981441189,
-2.32113634392463,-2.28999636926658,-2.24523770428675,-2.24339978367346,
-2.2426115934094,-2.24203809175711,-2.24150824322023,-2.24078347253271,
-2.23934824538023,-2.22751683458497,-2.22672374948812,-2.22625590958104,
-2.22534800975359,-2.22502344831907,-2.22113716132625,-2.18275914630555,
-2.13176431553918,-2.09043712840539,-2.08392676831173,-2.08208469087454,
-2.0809635546848,-2.07995271338379,-2.07866373999067,-2.07603913084501,
-2.06013541600145,-2.05912597775413,-2.05789746442295,-2.05637984014076,
-2.05038603877782,-2.03165219500241,-1.98163923476699,-1.92445196027978,
-1.92098419639131,-1.91993098190839,-1.91936371563633,-1.91880300556955,
-1.91811309626095,-1.91678617685548,-1.90847981233839,-1.89022752324672,
-1.86510097871217,-1.78698163973076,-1.78271435085037,-1.78047239538417,
-1.77925380751239,-1.7774899168109,-1.77541488075755,-1.77202302902228,
-1.76895602377055,-1.76688930463986,-1.76092432549067,-1.75906436135799,
-1.75805174185547,-1.75704650091625,-1.75582139500518,-1.75350588082379,
-1.74005698106839,-1.72772965008905,-1.71007710929056,-1.66077617355242,
-1.60153062805088,-1.59796854243598,-1.59690422779246,-1.59633472984669,
-1.59578534133915,-1.59511830953969,-1.59439907699419,-1.59326799968654,
-1.59110967661637,-1.57106541423971,-1.55791393435228,-1.47568369615516,
-1.44015068004721,-1.43695458447562,-1.43566306983383,-1.43471374148678,
-1.43368815381629,-1.43229938483529,-1.42915028519991,-1.42494178434964,
-1.38492566727802,-1.37066776653293),.UNSPECIFIED.);
#246=B_SPLINE_CURVE_WITH_KNOTS('',3,(#43780,#43781,#43782,#43783,#43784,
#43785,#43786,#43787,#43788,#43789,#43790,#43791,#43792,#43793,#43794,#43795,
#43796,#43797,#43798,#43799,#43800,#43801,#43802,#43803,#43804,#43805,#43806,
#43807,#43808,#43809,#43810,#43811,#43812,#43813,#43814,#43815,#43816,#43817,
#43818,#43819,#43820,#43821,#43822,#43823,#43824,#43825,#43826,#43827,#43828,
#43829,#43830,#43831,#43832,#43833,#43834,#43835,#43836,#43837,#43838,#43839,
#43840,#43841,#43842,#43843,#43844,#43845,#43846,#43847,#43848,#43849,#43850,
#43851,#43852,#43853,#43854,#43855,#43856,#43857,#43858,#43859,#43860,#43861,
#43862,#43863,#43864,#43865,#43866,#43867,#43868,#43869,#43870,#43871,#43872,
#43873,#43874,#43875,#43876,#43877,#43878,#43879,#43880,#43881,#43882,#43883,
#43884,#43885,#43886,#43887,#43888,#43889,#43890,#43891),.UNSPECIFIED.,
 .F.,.F.,(4,2,2,2,2,2,2,2,2,2,2,2,2,2,2,2,2,2,2,2,2,2,2,2,2,2,2,2,2,2,2,
2,2,2,2,2,2,2,2,2,2,2,2,2,2,2,2,2,2,2,2,2,2,2,2,4),(-0.662206116423806,
-0.662137559750041,-0.661470855298611,-0.660752004993613,-0.659621891659609,
-0.657466178368891,-0.652277035860876,-0.63744171206928,-0.624293750850653,
-0.542500520295884,-0.506513522013831,-0.503307672129327,-0.502014398124426,
-0.501064561315932,-0.500039175347543,-0.498652004379523,-0.495512173336552,
-0.440164470154991,-0.429877117309386,-0.421441133205797,-0.414280150821569,
-0.408066434356903,-0.390096250308862,-0.36430290480305,-0.34258084571345,
-0.340748638878288,-0.3400199847707,-0.339489128833762,-0.338927878080486,
-0.33821177337931,-0.33738592326876,-0.33599879987426,-0.333144731416516,
-0.325548652403063,-0.303261682945464,-0.187046472407577,-0.181019307651192,
-0.179151964421858,-0.178137994222143,-0.17713309747737,-0.175910848293904,
-0.173608024962096,-0.16042186776298,-0.138243228604426,-0.100181521156588,
-0.0328147580883714,-0.0293606617536357,-0.0188857287964917,-0.0175003670608609,
-0.0167884398410369,-0.0162619461170664,-0.0157295202875011,-0.0151663174959569,
-0.0144172166227127,-0.0132147540621359,-0.00096088211313939),
 .UNSPECIFIED.);
#247=B_SPLINE_CURVE_WITH_KNOTS('',3,(#43892,#43893,#43894,#43895,#43896,
#43897,#43898,#43899,#43900,#43901,#43902,#43903,#43904,#43905,#43906,#43907,
#43908,#43909,#43910,#43911,#43912,#43913,#43914,#43915,#43916,#43917,#43918,
#43919,#43920,#43921,#43922,#43923,#43924,#43925,#43926,#43927,#43928,#43929,
#43930,#43931,#43932,#43933,#43934,#43935,#43936,#43937,#43938,#43939,#43940,
#43941,#43942,#43943,#43944,#43945,#43946,#43947,#43948,#43949,#43950,#43951,
#43952,#43953,#43954,#43955,#43956,#43957,#43958,#43959,#43960,#43961,#43962,
#43963,#43964,#43965,#43966,#43967,#43968,#43969,#43970,#43971,#43972,#43973,
#43974,#43975,#43976,#43977,#43978,#43979,#43980,#43981,#43982,#43983,#43984,
#43985,#43986,#43987,#43988,#43989,#43990,#43991,#43992,#43993,#43994,#43995,
#43996,#43997,#43998,#43999,#44000,#44001,#44002,#44003,#44004,#44005,#44006,
#44007,#44008,#44009,#44010,#44011,#44012,#44013,#44014,#44015,#44016,#44017,
#44018,#44019,#44020,#44021,#44022,#44023,#44024,#44025,#44026,#44027,#44028,
#44029,#44030,#44031,#44032,#44033,#44034,#44035,#44036,#44037,#44038,#44039,
#44040,#44041,#44042,#44043,#44044,#44045,#44046,#44047,#44048,#44049,#44050,
#44051,#44052,#44053,#44054,#44055,#44056,#44057,#44058,#44059,#44060,#44061,
#44062,#44063,#44064,#44065,#44066,#44067,#44068,#44069,#44070,#44071,#44072,
#44073,#44074,#44075,#44076,#44077,#44078,#44079,#44080,#44081,#44082,#44083,
#44084,#44085,#44086,#44087,#44088,#44089,#44090,#44091,#44092,#44093,#44094,
#44095,#44096,#44097,#44098,#44099,#44100,#44101,#44102,#44103,#44104,#44105,
#44106,#44107),.UNSPECIFIED.,.F.,.F.,(4,2,2,2,2,2,2,2,2,2,2,2,2,2,2,2,2,
2,2,2,2,2,2,2,2,2,2,2,2,2,2,2,2,2,2,2,2,2,2,2,2,2,2,2,2,2,2,2,2,2,2,2,2,
2,2,2,2,2,2,2,2,2,2,2,2,2,2,2,2,2,2,2,2,2,2,2,2,2,2,2,2,2,2,2,2,2,2,2,2,
2,2,2,2,2,2,2,2,2,2,2,2,2,2,2,2,2,2,4),(-4.06206535738935,-3.97005035195392,
-3.93532834806842,-3.92009277866108,-3.91770192381126,-3.91646144925626,
-3.9154651797298,-3.91431787006135,-3.9123564003393,-3.90551022367957,-3.90179718679256,
-3.90021178661866,-3.89942353102071,-3.89828306951866,-3.89763928331943,
-3.89556052258089,-3.89404019770954,-3.89283571977218,-3.89152072187029,
-3.88537296495507,-3.79474634673191,-3.76845098056662,-3.76069391311167,
-3.75779617436791,-3.75639375423261,-3.75556177277186,-3.7548135137795,
-3.75425472747258,-3.75372088014253,-3.75298003247016,-3.75148007628766,
-3.73760814400221,-3.7121544153632,-3.6897927442744,-3.64578019267646,-3.61652637292871,
-3.59748865186431,-3.59496743894511,-3.59369986043141,-3.5927867611743,
-3.59181881259745,-3.59045555303582,-3.58763192109274,-3.5573149981734,
-3.47018363921452,-3.45696206231222,-3.44163717599157,-3.43648127401355,
-3.43433616112414,-3.43321027622464,-3.43225493001972,-3.43165208672577,
-3.43109949803665,-3.43036873264978,-3.42879866431127,-3.41756485950941,
-3.36523111801977,-3.3133785512979,-3.27907545344096,-3.27326642996472,
-3.27149976574654,-3.27039584794461,-3.26938126812184,-3.26808216638591,
-3.26533331483837,-3.2467336421036,-3.24521126105597,-3.23855574869198,
-3.14938095713286,-3.12410205319073,-3.11540569192217,-3.11225435038609,
-3.11076259053383,-3.10989396181372,-3.10911978216742,-3.10855609704119,
-3.10802882251451,-3.10731356852286,-3.10591503667278,-3.0950923809918,
-3.09346368105756,-3.09303336517969,-3.08481470087977,-3.04234389695859,
-2.98311607405423,-2.96482869096398,-2.95134638946022,-2.94902993315509,
-2.94780488744436,-2.94679998408651,-2.94578794757581,-2.94392975562866,
-2.93797589985788,-2.82139320316555,-2.80387383085411,-2.78970630072558,
-2.78794202482143,-2.78696383546038,-2.78611149818159,-2.78553171105634,
-2.78495840664869,-2.7842679874125,-2.78254828931893,-2.76695288708008,
-2.76594527306988,-2.76304764473065,-2.6999573776292,-2.69323737458904),
 .UNSPECIFIED.);
#248=B_SPLINE_CURVE_WITH_KNOTS('',3,(#44113,#44114,#44115,#44116,#44117,
#44118,#44119,#44120,#44121,#44122,#44123,#44124,#44125,#44126,#44127,#44128,
#44129,#44130,#44131,#44132,#44133,#44134,#44135,#44136,#44137,#44138,#44139,
#44140,#44141,#44142,#44143,#44144,#44145,#44146,#44147,#44148,#44149,#44150,
#44151,#44152,#44153,#44154,#44155,#44156,#44157,#44158,#44159,#44160,#44161,
#44162,#44163,#44164,#44165,#44166,#44167,#44168,#44169,#44170,#44171,#44172,
#44173,#44174,#44175,#44176,#44177,#44178,#44179,#44180,#44181,#44182,#44183,
#44184,#44185,#44186,#44187,#44188,#44189,#44190,#44191,#44192,#44193,#44194,
#44195,#44196,#44197,#44198,#44199,#44200,#44201,#44202,#44203,#44204,#44205,
#44206,#44207,#44208,#44209,#44210,#44211,#44212,#44213,#44214,#44215,#44216,
#44217,#44218,#44219,#44220,#44221,#44222,#44223,#44224,#44225,#44226,#44227,
#44228,#44229,#44230,#44231,#44232,#44233,#44234,#44235,#44236,#44237,#44238,
#44239,#44240,#44241,#44242,#44243,#44244,#44245,#44246,#44247,#44248,#44249,
#44250,#44251,#44252,#44253,#44254,#44255,#44256,#44257,#44258,#44259,#44260,
#44261,#44262,#44263,#44264,#44265,#44266,#44267,#44268,#44269,#44270,#44271,
#44272,#44273,#44274,#44275,#44276,#44277,#44278,#44279,#44280,#44281,#44282,
#44283,#44284,#44285,#44286,#44287,#44288,#44289,#44290,#44291,#44292,#44293,
#44294,#44295,#44296,#44297,#44298,#44299,#44300,#44301,#44302,#44303,#44304),
 .UNSPECIFIED.,.F.,.F.,(4,2,2,2,2,2,2,2,2,2,2,2,2,2,2,2,2,2,2,2,2,2,2,2,
2,2,2,2,2,2,2,2,2,2,2,2,2,2,2,2,2,2,2,2,2,2,2,2,2,2,2,2,2,2,2,2,2,2,2,2,
2,2,2,2,2,2,2,2,2,2,2,2,2,2,2,2,2,2,2,2,2,2,2,2,2,2,2,2,2,2,2,2,2,2,2,4),
(-1.36992249076833,-1.36011110780835,-1.25889637125947,-1.25294780947012,
-1.2510904907751,-1.25007875752745,-1.24917412830259,-1.24801559320514,
-1.24597610048891,-1.24348253171853,-1.18581330666231,-1.09496916055279,
-1.09043233882278,-1.08923357519539,-1.08850558129432,-1.087939951584,-1.08731938653578,
-1.08630835283231,-1.08282480737874,-1.06039988309063,-1.03573485910554,
-0.937333701723687,-0.935904705376236,-0.929870643654192,-0.928002805115158,
-0.926988929954721,-0.926082840215784,-0.924926547731394,-0.922893745984984,
-0.920412645899742,-0.915339463228706,-0.902057370512905,-0.870245011814187,
-0.782618756168538,-0.781186474648235,-0.779696680472317,-0.767794444789422,
-0.766198215635278,-0.765462459288475,-0.764895679749286,-0.76427890352718,
-0.763284785671746,-0.759958400337259,-0.739174741858444,-0.690284340083477,
-0.628460401749236,-0.626947282274918,-0.625752345461889,-0.62222189780312,
-0.621688193249525,-0.617945436550069,-0.614474046058225,-0.613068644374581,
-0.606955283329361,-0.605077698695959,-0.604061785125997,-0.603154284414437,
-0.601999893488966,-0.600115643836136,-0.59776079546241,-0.593034763496795,
-0.580960922147294,-0.557852139939544,-0.450972812757739,-0.446286472258731,
-0.443614844829819,-0.442666671045137,-0.442120612001335,-0.441612255071038,
-0.440908125447865,-0.439512379391033,-0.42929114893009,-0.402499694111724,
-0.36393595292225,-0.343766784911088,-0.314011641336004,-0.285879911581213,
-0.282799963399097,-0.28156141959571,-0.280531630626738,-0.27958552795347,
-0.278555517000745,-0.27597202056229,-0.254197331456896,-0.231034098351554,
-0.180770198187209,-0.124383207341576,-0.120907155426492,-0.119853034392882,
-0.119285629371723,-0.11872500801893,-0.118035535392214,-0.116710451095787,
-0.108445529041699,-0.0905574676002597,-0.000962469125110394),
 .UNSPECIFIED.);
#249=B_SPLINE_CURVE_WITH_KNOTS('',3,(#44305,#44306,#44307,#44308,#44309,
#44310,#44311,#44312,#44313,#44314,#44315,#44316,#44317,#44318,#44319,#44320,
#44321,#44322,#44323,#44324,#44325,#44326,#44327,#44328,#44329,#44330,#44331,
#44332,#44333,#44334,#44335,#44336,#44337,#44338,#44339,#44340,#44341,#44342,
#44343,#44344,#44345,#44346,#44347,#44348,#44349,#44350,#44351,#44352,#44353,
#44354,#44355,#44356,#44357,#44358,#44359,#44360,#44361,#44362,#44363,#44364,
#44365,#44366,#44367,#44368,#44369,#44370,#44371,#44372,#44373,#44374,#44375,
#44376,#44377,#44378,#44379,#44380,#44381,#44382,#44383,#44384,#44385,#44386,
#44387,#44388,#44389,#44390,#44391,#44392,#44393,#44394,#44395,#44396,#44397,
#44398,#44399,#44400,#44401,#44402,#44403,#44404,#44405,#44406,#44407,#44408,
#44409,#44410,#44411,#44412,#44413,#44414,#44415,#44416,#44417,#44418,#44419,
#44420,#44421,#44422,#44423,#44424,#44425,#44426),.UNSPECIFIED.,.F.,.F.,
(4,2,2,2,2,2,2,2,2,2,2,2,2,2,2,2,2,2,2,2,2,2,2,2,2,2,2,2,2,2,2,2,2,2,2,
2,2,2,2,2,2,2,2,2,2,2,2,2,2,2,2,2,2,2,2,2,2,2,2,2,4),(-4.06307029976562,
-4.02621299276285,-4.02351802668358,-4.02194888577496,-4.02084961439851,
-4.01990644418212,-4.01889549160324,-4.01760594727514,-4.01497868571737,
-3.99902422831513,-3.99585419476142,-3.99241343008694,-3.98020157012189,
-3.97450569539038,-3.95242825469067,-3.86361183675127,-3.85981994263567,
-3.85877727241304,-3.85814938065569,-3.85758516285388,-3.85685777469768,
-3.85534718577422,-3.84551021456565,-3.84321483263195,-3.84105582799669,
-3.84059377470798,-3.7501971763093,-3.71980593390042,-3.70724718831045,
-3.69985500085665,-3.69793344300521,-3.69697150209076,-3.69596631676996,
-3.69495132848865,-3.6930800092665,-3.6870233357477,-3.6810663273813,-3.67866874590036,
-3.67658730112641,-3.67479280671131,-3.67357143020716,-3.66934688360038,
-3.658927640011,-3.61079023431505,-3.60549406522702,-3.59946617655345,-3.59250114127332,
-3.5842550103788,-3.55574833781797,-3.54329178305896,-3.53705746829144,
-3.53583174019658,-3.53516340804141,-3.53465857398292,-3.53409334467418,
-3.53305032356407,-3.52966759537004,-3.52804086828078,-3.44207330605695,
-3.40199142588857,-3.40146716175795),.UNSPECIFIED.);
#250=B_SPLINE_CURVE_WITH_KNOTS('',3,(#44427,#44428,#44429,#44430,#44431,
#44432,#44433,#44434,#44435,#44436,#44437,#44438,#44439,#44440,#44441,#44442,
#44443,#44444,#44445,#44446,#44447,#44448,#44449,#44450,#44451,#44452,#44453,
#44454,#44455,#44456,#44457,#44458,#44459,#44460,#44461,#44462,#44463,#44464,
#44465,#44466,#44467,#44468,#44469,#44470,#44471,#44472,#44473,#44474,#44475,
#44476,#44477,#44478,#44479,#44480,#44481,#44482,#44483,#44484,#44485,#44486,
#44487,#44488,#44489,#44490,#44491,#44492,#44493,#44494,#44495,#44496,#44497,
#44498,#44499,#44500,#44501,#44502,#44503,#44504,#44505,#44506,#44507,#44508,
#44509,#44510,#44511,#44512,#44513,#44514,#44515,#44516,#44517,#44518,#44519,
#44520,#44521,#44522,#44523,#44524,#44525,#44526,#44527,#44528,#44529,#44530,
#44531,#44532,#44533,#44534,#44535,#44536,#44537,#44538,#44539,#44540,#44541,
#44542,#44543,#44544,#44545,#44546,#44547,#44548,#44549,#44550,#44551,#44552,
#44553,#44554,#44555,#44556,#44557,#44558,#44559,#44560,#44561,#44562,#44563,
#44564,#44565,#44566,#44567,#44568,#44569,#44570,#44571,#44572,#44573,#44574,
#44575,#44576,#44577,#44578,#44579,#44580,#44581,#44582,#44583,#44584,#44585,
#44586,#44587,#44588,#44589,#44590,#44591,#44592,#44593,#44594,#44595,#44596,
#44597,#44598,#44599,#44600,#44601,#44602,#44603,#44604,#44605,#44606,#44607,
#44608,#44609,#44610,#44611,#44612,#44613,#44614,#44615,#44616,#44617,#44618,
#44619,#44620,#44621,#44622,#44623,#44624,#44625,#44626,#44627,#44628,#44629,
#44630,#44631,#44632,#44633,#44634,#44635,#44636,#44637,#44638,#44639,#44640,
#44641,#44642,#44643,#44644,#44645,#44646,#44647,#44648,#44649,#44650,#44651,
#44652,#44653,#44654,#44655,#44656,#44657,#44658,#44659,#44660,#44661,#44662,
#44663,#44664,#44665,#44666,#44667,#44668,#44669,#44670,#44671,#44672,#44673,
#44674,#44675,#44676,#44677,#44678,#44679,#44680,#44681,#44682,#44683,#44684,
#44685,#44686,#44687,#44688,#44689,#44690,#44691,#44692,#44693,#44694,#44695,
#44696,#44697,#44698,#44699,#44700,#44701,#44702,#44703,#44704,#44705,#44706,
#44707,#44708,#44709,#44710,#44711,#44712,#44713,#44714,#44715,#44716,#44717,
#44718,#44719,#44720,#44721,#44722,#44723,#44724,#44725,#44726,#44727,#44728,
#44729,#44730,#44731,#44732,#44733,#44734,#44735,#44736,#44737,#44738,#44739,
#44740,#44741,#44742,#44743,#44744,#44745,#44746,#44747,#44748,#44749,#44750,
#44751,#44752),.UNSPECIFIED.,.F.,.F.,(4,2,2,2,2,2,2,2,2,2,2,2,2,2,2,2,2,
2,2,2,2,2,2,2,2,2,2,2,2,2,2,2,2,2,2,2,2,2,2,2,2,2,2,2,2,2,2,2,2,2,2,2,2,
2,2,2,2,2,2,2,2,2,2,2,2,2,2,2,2,2,2,2,2,2,2,2,2,2,2,2,2,2,2,2,2,2,2,2,2,
2,2,2,2,2,2,2,2,2,2,2,2,2,2,2,2,2,2,2,2,2,2,2,2,2,2,2,2,2,2,2,2,2,2,2,2,
2,2,2,2,2,2,2,2,2,2,2,2,2,2,2,2,2,2,2,2,2,2,2,2,2,2,2,2,2,2,2,2,2,2,2,2,
2,4),(-2.69323737458904,-2.66695066000876,-2.64182901214515,-2.62819742798369,
-2.62587365866223,-2.62464686156451,-2.62364161081488,-2.62263014466621,
-2.62077563918824,-2.61485408885999,-2.61340434843227,-2.60983489595764,
-2.60626296557934,-2.60577036973392,-2.60366771636178,-2.60264295115914,
-2.60140188674851,-2.59960099323394,-2.59336206742085,-2.50234334390139,
-2.48184443833446,-2.4667959525035,-2.46496963966017,-2.46396693279606,
-2.46330158542213,-2.46267277427215,-2.46212425303578,-2.46142625489302,
-2.46035153700574,-2.45552133442309,-2.36172357025586,-2.3377499186391,
-2.309067134064,-2.30387260323175,-2.30217804510313,-2.30108986212082,-2.30006911586781,
-2.29873274159437,-2.29648534228126,-2.28291394277717,-2.28085154492269,
-2.27898490544721,-2.27442044479301,-2.27357292427173,-2.26183265851919,
-2.25616222555116,-2.19069619573504,-2.16639214407842,-2.14457891796077,
-2.14115312409478,-2.14014798829007,-2.13952859952953,-2.13896235204922,
-2.13823127332206,-2.13666057307168,-2.1254234763837,-2.0321312895758,-2.01041273211509,
-2.00163695316889,-1.99852579826467,-1.982476473502,-1.97984477492052,-1.97855448196252,
-1.97754359859112,-1.97642343478984,-1.97458527985579,-1.96811198895223,
-1.92716989925069,-1.87634647579663,-1.86635080849869,-1.82087757123191,
-1.81804251040804,-1.81707074987542,-1.81651995602071,-1.8160128740924,
-1.81531908673249,-1.81397335733894,-1.8051904272082,-1.78434856242143,
-1.73562894792959,-1.66236926545113,-1.65778956345497,-1.65611895174762,
-1.65514439910985,-1.65415199122443,-1.65288549578109,-1.65150174381603,
-1.64925396753122,-1.64481821807107,-1.60091271802256,-1.50929577850373,
-1.50837720442649,-1.50653385129321,-1.49594631052236,-1.4945563899444,
-1.49384321864254,-1.49331634294621,-1.49274042350044,-1.49193899746327,
-1.49002448480513,-1.48738919481383,-1.45903719466622,-1.34043780707141,
-1.33476307113318,-1.33293987105367,-1.33193481456781,-1.33094916436177,
-1.32974697238497,-1.32845219750689,-1.32641600555728,-1.32254078035876,
-1.28772232709118,-1.1905936034179,-1.18943639177376,-1.18809675704507,
-1.18640008761606,-1.17277676271892,-1.17128371566986,-1.17054439268769,
-1.1700107624716,-1.16943993991893,-1.1686669546663,-1.16691428134074,-1.13222330163187,
-1.01799281189823,-1.01162488132412,-1.00971696749924,-1.00858130290577,
-1.00759102564218,-1.00636135633456,-1.00399381690932,-1.00100551847271,
-0.994484739329017,-0.975873751621818,-0.92554955569963,-0.882694056078951,
-0.850188952980269,-0.848184973688339,-0.847427826112266,-0.846889503149032,
-0.846378360691303,-0.845654623392182,-0.844161440014647,-0.830065530139632,
-0.803250616064687,-0.793092442361747,-0.707915666286649,-0.706669354137044,
-0.705616502074262,-0.703532826701615,-0.70294124217594,-0.70131107551983,
-0.700467005634569,-0.695091100936416,-0.688697051917372,-0.686786176338426,
-0.685649896998808,-0.68465931120268,-0.683430427098059,-0.681066347591054,
-0.678083554983827,-0.67157879553533,-0.662484546563834),.UNSPECIFIED.);
#251=B_SPLINE_CURVE_WITH_KNOTS('',3,(#44757,#44758,#44759,#44760,#44761,
#44762,#44763,#44764,#44765,#44766,#44767,#44768,#44769,#44770,#44771,#44772,
#44773,#44774,#44775,#44776,#44777,#44778,#44779,#44780,#44781,#44782,#44783,
#44784,#44785,#44786,#44787,#44788,#44789,#44790,#44791,#44792,#44793,#44794,
#44795,#44796,#44797,#44798,#44799,#44800,#44801,#44802,#44803,#44804,#44805,
#44806,#44807,#44808,#44809,#44810,#44811,#44812,#44813,#44814,#44815,#44816,
#44817,#44818,#44819,#44820,#44821,#44822,#44823,#44824,#44825,#44826,#44827,
#44828,#44829,#44830,#44831,#44832,#44833,#44834,#44835,#44836,#44837,#44838,
#44839,#44840,#44841,#44842,#44843,#44844,#44845,#44846,#44847,#44848,#44849,
#44850,#44851,#44852,#44853,#44854,#44855,#44856,#44857,#44858,#44859,#44860,
#44861,#44862,#44863,#44864,#44865,#44866,#44867,#44868,#44869,#44870,#44871,
#44872,#44873,#44874,#44875,#44876,#44877,#44878,#44879,#44880,#44881,#44882,
#44883,#44884,#44885,#44886,#44887,#44888,#44889,#44890,#44891,#44892,#44893,
#44894,#44895,#44896,#44897,#44898,#44899,#44900,#44901,#44902,#44903,#44904,
#44905,#44906,#44907,#44908,#44909,#44910,#44911,#44912,#44913,#44914,#44915,
#44916,#44917,#44918,#44919,#44920,#44921,#44922,#44923,#44924,#44925,#44926,
#44927,#44928,#44929,#44930,#44931,#44932,#44933,#44934,#44935,#44936,#44937,
#44938,#44939,#44940,#44941,#44942,#44943,#44944,#44945,#44946,#44947,#44948,
#44949,#44950,#44951,#44952,#44953,#44954,#44955,#44956,#44957,#44958,#44959,
#44960,#44961,#44962,#44963,#44964,#44965,#44966,#44967,#44968,#44969,#44970,
#44971,#44972,#44973,#44974,#44975,#44976,#44977,#44978,#44979,#44980,#44981,
#44982,#44983,#44984,#44985,#44986,#44987,#44988,#44989,#44990,#44991,#44992,
#44993,#44994,#44995,#44996,#44997,#44998,#44999,#45000,#45001,#45002,#45003,
#45004,#45005,#45006,#45007,#45008,#45009,#45010,#45011,#45012,#45013,#45014,
#45015,#45016,#45017,#45018,#45019,#45020,#45021,#45022,#45023,#45024,#45025,
#45026,#45027,#45028,#45029,#45030,#45031,#45032,#45033,#45034,#45035,#45036,
#45037,#45038,#45039,#45040,#45041,#45042,#45043,#45044,#45045,#45046,#45047,
#45048,#45049,#45050,#45051,#45052,#45053,#45054),.UNSPECIFIED.,.F.,.F.,
(4,2,2,2,2,2,2,2,2,2,2,2,2,2,2,2,2,2,2,2,2,2,2,2,2,2,2,2,2,2,2,2,2,2,2,
2,2,2,2,2,2,2,2,2,2,2,2,2,2,2,2,2,2,2,2,2,2,2,2,2,2,2,2,2,2,2,2,2,2,2,2,
2,2,2,2,2,2,2,2,2,2,2,2,2,2,2,2,2,2,2,2,2,2,2,2,2,2,2,2,2,2,2,2,2,2,2,2,
2,2,2,2,2,2,2,2,2,2,2,2,2,2,2,2,2,2,2,2,2,2,2,2,2,2,2,2,2,2,2,2,2,2,2,2,
2,2,2,2,2,4),(-3.39990203970593,-3.37568906292057,-3.36178630294155,-3.35163759979921,
-3.35024913805766,-3.34968079191137,-3.34910709431136,-3.34857802843084,
-3.34785574102047,-3.3464296852929,-3.33484958607241,-3.30149814682876,
-3.26159896141466,-3.22265935806477,-3.20455103077339,-3.19201001310503,
-3.18964468023475,-3.18840929853978,-3.18750023590305,-3.18651823802952,
-3.18510422651216,-3.18114853425714,-3.11655674766835,-3.06673347130353,
-3.0404772553221,-3.02884269113632,-3.027411557059,-3.02669438297866,-3.02618427136127,
-3.02564362271037,-3.02472231361015,-3.02223352100496,-2.98260003124754,
-2.91609331838607,-2.88373338373485,-2.8692239675763,-2.86683869631314,
-2.86556825167259,-2.86465458301084,-2.86368741516949,-2.86232751883703,
-2.85951819628024,-2.82983250978034,-2.80928534262578,-2.74762095988082,
-2.72413258429119,-2.7079193107732,-2.70601309502644,-2.70454878279257,
-2.70383327423822,-2.70332112551669,-2.70278506082854,-2.70203621458432,
-2.70008318562765,-2.67136002289411,-2.58879484883179,-2.55129231134297,
-2.54517484565672,-2.5433610484862,-2.54224655677649,-2.54123476772663,
-2.53993493394394,-2.53725417524231,-2.52907243441431,-2.52671370613265,
-2.52388209052998,-2.52339295894234,-2.5209792169163,-2.51741852649105,
-2.4345715629149,-2.3841832292528,-2.38189930753702,-2.38104096065967,-2.38045008863287,
-2.37987642844745,-2.3791842871541,-2.37745351298012,-2.36146004118226,
-2.33219007892715,-2.31235187782139,-2.27212882893557,-2.24263988041179,
-2.22351154050838,-2.22098709892768,-2.21971864546848,-2.21880521223288,
-2.21783718462719,-2.21619915865981,-2.21183064819459,-2.2058618658656,
-2.09688310266205,-2.06056329815115,-2.0586677209403,-2.05786957990353,
-2.0572943119063,-2.05676679756776,-2.05605098037175,-2.05465064338855,
-2.04378747323072,-2.0421904443236,-2.04176360829486,-2.04056307446308,
-2.04007259737402,-2.03788385830732,-2.03673449151926,-2.03136324915038,
-2.01007514577286,-1.90535919762152,-1.89910701639322,-1.89721265573857,
-1.89619325713786,-1.89519837114668,-1.89398902825268,-1.89174642253287,
-1.87975764426959,-1.85612378776406,-1.81078635856992,-1.77840572855741,
-1.75067383698808,-1.73713546906084,-1.73550164719207,-1.73481480908172,
-1.73424250003767,-1.73364971557648,-1.73276468552204,-1.73031223694464,
-1.68808944411968,-1.58218257604977,-1.576018733314,-1.57413511759528,-1.57311800875414,
-1.57213365790823,-1.57095013865604,-1.56879308827265,-1.56612741964831,
-1.51587941804059,-1.4514926255499,-1.43579834140671,-1.42815852180856,
-1.42502264431835,-1.41391464536443,-1.41236949675846,-1.41163251925625,
-1.41106556036876,-1.41044937286506,-1.40945785552894,-1.40615495541566,
-1.38561133259827,-1.36992249076833),.UNSPECIFIED.);
#252=B_SPLINE_CURVE_WITH_KNOTS('',3,(#45056,#45057,#45058,#45059,#45060,
#45061,#45062,#45063,#45064,#45065,#45066,#45067,#45068,#45069,#45070,#45071,
#45072,#45073,#45074,#45075,#45076,#45077,#45078,#45079,#45080,#45081,#45082,
#45083,#45084,#45085,#45086,#45087,#45088,#45089,#45090,#45091,#45092,#45093,
#45094,#45095,#45096,#45097,#45098,#45099,#45100,#45101,#45102,#45103,#45104,
#45105,#45106,#45107,#45108,#45109,#45110,#45111,#45112,#45113,#45114,#45115,
#45116,#45117,#45118,#45119,#45120,#45121,#45122,#45123,#45124,#45125,#45126,
#45127,#45128,#45129,#45130,#45131,#45132,#45133,#45134,#45135,#45136,#45137,
#45138,#45139,#45140,#45141,#45142,#45143,#45144,#45145,#45146,#45147,#45148,
#45149,#45150,#45151,#45152,#45153),.UNSPECIFIED.,.F.,.F.,(4,2,2,2,2,2,
2,2,2,2,2,2,2,2,2,2,2,2,2,2,2,2,2,2,2,2,2,2,2,2,2,2,2,2,2,2,2,2,2,2,2,2,
2,2,2,2,2,2,4),(-0.662484546563834,-0.653028498095685,-0.616296305791393,
-0.530572689536388,-0.52585539356106,-0.524790056139435,-0.524095078273972,
-0.523590265262604,-0.522961522669115,-0.521914295862368,-0.518072303520396,
-0.429445501281873,-0.389416394524991,-0.385848483951991,-0.382043981007247,
-0.379961831561385,-0.377784719650975,-0.375951484981409,-0.371982876524711,
-0.3656451265558,-0.363740750107707,-0.362605883695746,-0.361616042869752,
-0.360645537328616,-0.358626092820093,-0.350040855825288,-0.334735425516253,
-0.31016377779759,-0.207094952442866,-0.206424747570049,-0.202563246583696,
-0.201478129244575,-0.200834573400788,-0.200278453904849,-0.199579284473267,
-0.198207774530163,-0.188721050710403,-0.161933511971421,-0.0786882112168834,
-0.0730623105976422,-0.0444561768123828,-0.0413632162909043,-0.0401225427657687,
-0.039092206450294,-0.038145925876914,-0.0371166700067285,-0.0357235945869139,
-0.0334535663773804,-0.000960739771948738),.UNSPECIFIED.);
#253=B_SPLINE_CURVE_WITH_KNOTS('',3,(#45154,#45155,#45156,#45157,#45158,
#45159,#45160,#45161,#45162,#45163,#45164,#45165,#45166,#45167,#45168,#45169,
#45170,#45171,#45172,#45173,#45174,#45175,#45176,#45177,#45178,#45179,#45180,
#45181,#45182,#45183,#45184,#45185,#45186,#45187,#45188,#45189,#45190,#45191,
#45192,#45193,#45194,#45195,#45196,#45197,#45198,#45199,#45200,#45201,#45202,
#45203,#45204,#45205,#45206,#45207,#45208,#45209,#45210,#45211,#45212,#45213,
#45214,#45215,#45216,#45217,#45218,#45219,#45220,#45221,#45222,#45223,#45224,
#45225,#45226,#45227,#45228,#45229,#45230,#45231,#45232,#45233,#45234,#45235,
#45236,#45237,#45238,#45239,#45240,#45241,#45242,#45243,#45244,#45245,#45246,
#45247,#45248,#45249,#45250,#45251,#45252,#45253,#45254,#45255,#45256,#45257,
#45258,#45259,#45260,#45261,#45262,#45263,#45264,#45265,#45266,#45267,#45268,
#45269,#45270,#45271,#45272,#45273,#45274,#45275,#45276,#45277,#45278,#45279,
#45280,#45281,#45282,#45283,#45284,#45285,#45286,#45287,#45288,#45289,#45290,
#45291,#45292,#45293,#45294,#45295,#45296,#45297,#45298,#45299,#45300,#45301,
#45302,#45303,#45304,#45305,#45306,#45307,#45308,#45309,#45310,#45311,#45312,
#45313,#45314,#45315,#45316,#45317,#45318,#45319,#45320,#45321,#45322,#45323,
#45324,#45325,#45326,#45327,#45328,#45329,#45330,#45331,#45332,#45333,#45334,
#45335,#45336,#45337,#45338,#45339,#45340,#45341,#45342,#45343,#45344,#45345,
#45346,#45347,#45348,#45349,#45350,#45351,#45352,#45353,#45354,#45355,#45356,
#45357,#45358,#45359,#45360,#45361,#45362,#45363,#45364,#45365),
 .UNSPECIFIED.,.F.,.F.,(4,2,2,2,2,2,2,2,2,2,2,2,2,2,2,2,2,2,2,2,2,2,2,2,
2,2,2,2,2,2,2,2,2,2,2,2,2,2,2,2,2,2,2,2,2,2,2,2,2,2,2,2,2,2,2,2,2,2,2,2,
2,2,2,2,2,2,2,2,2,2,2,2,2,2,2,2,2,2,2,2,2,2,2,2,2,2,2,2,2,2,2,2,2,2,2,2,
2,2,2,2,2,2,2,2,2,4),(-4.06127014542011,-3.96345360342496,-3.94283348390587,
-3.93952285030901,-3.93853020035635,-3.93791358486381,-3.93734642573133,
-3.93660945330883,-3.93500775257484,-3.92297456255997,-3.91964322838868,
-3.91553485159133,-3.89332821618906,-3.82371342826044,-3.80332568387682,
-3.78837019164686,-3.77993305323193,-3.77792396121982,-3.77695419739667,
-3.77596229970356,-3.77482384076671,-3.77290436873306,-3.76643966492423,
-3.76252733835516,-3.76075659642063,-3.75861228680896,-3.75805872741368,
-3.75596890550248,-3.754513394651,-3.75330689379693,-3.75179249796371,-3.74654907053496,
-3.70546252060252,-3.67647570978518,-3.621584694545,-3.61680442532471,-3.61567611640045,
-3.61502918521708,-3.61446802297562,-3.61377078399619,-3.61269848456357,
-3.60789793005972,-3.5208927820507,-3.48975277665014,-3.46828555572928,
-3.46101937772421,-3.45778043762926,-3.45525407182727,-3.45398962808627,
-3.45301291496556,-3.45204014380962,-3.4503788919813,-3.44586142558242,
-3.37946486463497,-3.34335078923876,-3.31435012516755,-3.30199884003998,
-3.29406530542728,-3.29275426149695,-3.29206772633116,-3.29150722679693,
-3.29085198323463,-3.28971675234639,-3.2853641766045,-3.28489194433908,
-3.18717767572461,-3.15487352585317,-3.14146202439485,-3.13635137493903,
-3.13385646301956,-3.13181366392817,-3.13065513031136,-3.12974977265603,
-3.12873708912742,-3.12687639160503,-3.12090421733095,-3.0222096922247,
-2.97149035506671,-2.9697574436245,-2.96898801170755,-2.96841775426936,
-2.96788310458741,-2.96714002102135,-2.96563200765558,-2.96164652392502,
-2.86405329816224,-2.81726354181658,-2.81267347325761,-2.81036844251205,
-2.80896071799233,-2.80767583868822,-2.80668106832067,-2.8057127240601,
-2.80434905875503,-2.8015250793395,-2.79394275524369,-2.79213031421433,
-2.79006698799704,-2.78959526099725,-2.78776832304441,-2.78486689438122,
-2.78367028196406,-2.78211136428351,-2.77497173158081,-2.70666089636562,
-2.69202105007084),.UNSPECIFIED.);
#254=B_SPLINE_CURVE_WITH_KNOTS('',3,(#45371,#45372,#45373,#45374,#45375,
#45376,#45377,#45378,#45379,#45380,#45381,#45382,#45383,#45384,#45385,#45386,
#45387,#45388,#45389,#45390,#45391,#45392,#45393,#45394,#45395,#45396,#45397,
#45398,#45399,#45400,#45401,#45402,#45403,#45404,#45405,#45406,#45407,#45408,
#45409,#45410,#45411,#45412,#45413,#45414,#45415,#45416,#45417,#45418,#45419,
#45420,#45421,#45422,#45423,#45424,#45425,#45426,#45427,#45428,#45429,#45430,
#45431,#45432,#45433,#45434,#45435,#45436,#45437,#45438,#45439,#45440,#45441,
#45442,#45443,#45444,#45445,#45446,#45447,#45448,#45449,#45450,#45451,#45452,
#45453,#45454,#45455,#45456,#45457,#45458,#45459,#45460,#45461,#45462,#45463,
#45464,#45465,#45466,#45467,#45468,#45469,#45470,#45471,#45472,#45473,#45474,
#45475,#45476,#45477,#45478,#45479,#45480,#45481,#45482,#45483,#45484,#45485,
#45486,#45487,#45488,#45489,#45490,#45491,#45492,#45493,#45494,#45495,#45496,
#45497,#45498,#45499,#45500,#45501,#45502,#45503,#45504,#45505,#45506,#45507,
#45508,#45509,#45510,#45511,#45512,#45513,#45514,#45515,#45516,#45517,#45518,
#45519,#45520,#45521,#45522,#45523,#45524,#45525,#45526,#45527,#45528,#45529,
#45530,#45531,#45532,#45533,#45534,#45535,#45536,#45537,#45538,#45539,#45540,
#45541,#45542,#45543,#45544,#45545,#45546,#45547,#45548,#45549,#45550,#45551,
#45552,#45553,#45554,#45555,#45556,#45557,#45558,#45559,#45560,#45561,#45562,
#45563,#45564,#45565,#45566),.UNSPECIFIED.,.F.,.F.,(4,2,2,2,2,2,2,2,2,2,
2,2,2,2,2,2,2,2,2,2,2,2,2,2,2,2,2,2,2,2,2,2,2,2,2,2,2,2,2,2,2,2,2,2,2,2,
2,2,2,2,2,2,2,2,2,2,2,2,2,2,2,2,2,2,2,2,2,2,2,2,2,2,2,2,2,2,2,2,2,2,2,2,
2,2,2,2,2,2,2,2,2,2,2,2,2,2,2,4),(-1.37006013660576,-1.36813097394664,-1.32932735761755,
-1.25858965367075,-1.23057258816633,-1.2286296907977,-1.22788241632752,
-1.22734671185576,-1.22683424142332,-1.22628381396108,-1.22506538691945,
-1.21891329741473,-1.20664598041326,-1.18447910256005,-1.12913574310777,
-1.07220127763863,-1.06843097000159,-1.06704509530975,-1.06607074681383,
-1.06515933446729,-1.06390617936786,-1.06145644709069,-1.0449600251339,
-1.00540499266253,-0.948642773372128,-0.923369959339648,-0.921576008121546,
-0.921013266749065,-0.907176292643627,-0.905677023241927,-0.904936188773754,
-0.904402198413551,-0.903831706534511,-0.903269252454078,-0.901936509723686,
-0.893379634416647,-0.873530442476435,-0.82285787511113,-0.782778572925608,
-0.769472551448452,-0.747892324998544,-0.745023163405022,-0.743700878407185,
-0.742682511269694,-0.741588650353387,-0.73986813003035,-0.734576219552312,
-0.726427642784752,-0.7019191579815,-0.638150144149182,-0.593104736606286,
-0.592026402197716,-0.590438525618296,-0.587691367670873,-0.583398584783547,
-0.582269252407768,-0.581615414219628,-0.581054885802996,-0.580366775684865,
-0.579631751813795,-0.576372713280065,-0.551120999278779,-0.509290951689597,
-0.428199055692575,-0.426948300765325,-0.422686678420152,-0.421065428990359,
-0.420100607840701,-0.419185764988364,-0.417908260011066,-0.415339804907564,
-0.401805544246659,-0.373160373205551,-0.344796516450849,-0.318729689397913,
-0.2634067526509,-0.260186303972084,-0.259163340098403,-0.258602253954898,
-0.258040943342226,-0.257499355794066,-0.256814437868253,-0.255764953036627,
-0.242117344300038,-0.213585554864005,-0.202494970741812,-0.190429095569164,
-0.105563197169878,-0.10007101334907,-0.0982715601255558,-0.0972712814648368,
-0.0962744536600228,-0.0950325528330217,-0.0926366420268566,-0.0896360550492344,
-0.0830792676873454,-0.064331162693157,-0.000961908199084628),
 .UNSPECIFIED.);
#255=B_SPLINE_CURVE_WITH_KNOTS('',3,(#45567,#45568,#45569,#45570,#45571,
#45572,#45573,#45574,#45575,#45576,#45577,#45578,#45579,#45580,#45581,#45582,
#45583,#45584,#45585,#45586,#45587,#45588,#45589,#45590,#45591,#45592,#45593,
#45594,#45595,#45596,#45597,#45598,#45599,#45600,#45601,#45602,#45603,#45604,
#45605,#45606,#45607,#45608,#45609,#45610,#45611,#45612,#45613,#45614,#45615,
#45616,#45617,#45618,#45619,#45620,#45621,#45622,#45623,#45624,#45625,#45626,
#45627,#45628,#45629,#45630,#45631,#45632,#45633,#45634,#45635,#45636,#45637,
#45638,#45639,#45640,#45641,#45642,#45643,#45644,#45645,#45646,#45647,#45648,
#45649,#45650,#45651,#45652,#45653,#45654,#45655,#45656,#45657,#45658,#45659,
#45660,#45661,#45662,#45663,#45664,#45665,#45666),.UNSPECIFIED.,.F.,.F.,
(4,2,2,2,2,2,2,2,2,2,2,2,2,2,2,2,2,2,2,2,2,2,2,2,2,2,2,2,2,2,2,2,2,2,2,
2,2,2,2,2,2,2,2,2,2,2,2,2,2,4),(-4.06049778996915,-3.99904159918256,-3.99731369694622,
-3.9963500425661,-3.99570114292148,-3.99507440656776,-3.99451040376592,
-3.99378216471943,-3.99226578783663,-3.9822865548596,-3.97986840961498,
-3.9306046388084,-3.92206896077134,-3.91472479405678,-3.89982315449474,
-3.85857816609013,-3.84034738026085,-3.83756243007123,-3.83530728122348,
-3.83409538755797,-3.83318886045351,-3.83219501848855,-3.83042688977888,
-3.82516666684674,-3.74360937424023,-3.72094211655588,-3.6948261901867,
-3.6809871027978,-3.67654913659154,-3.67368182493792,-3.67297483167414,
-3.67230687904806,-3.67180230047736,-3.67123732474311,-3.67019468043799,
-3.66681244995404,-3.61070253090208,-3.5656812649305,-3.55851304448269,
-3.53012041321281,-3.51497189534137,-3.51324871903817,-3.51172019812485,
-3.51066802158057,-3.50963790876059,-3.50839735908715,-3.5053039533476,
-3.47665769918529,-3.42568494445762,-3.39990203970593),.UNSPECIFIED.);
#256=B_SPLINE_CURVE_WITH_KNOTS('',3,(#45667,#45668,#45669,#45670,#45671,
#45672,#45673,#45674,#45675,#45676,#45677,#45678,#45679,#45680,#45681,#45682,
#45683,#45684,#45685,#45686,#45687,#45688,#45689,#45690,#45691,#45692,#45693,
#45694,#45695,#45696,#45697,#45698,#45699,#45700,#45701,#45702,#45703,#45704,
#45705,#45706,#45707,#45708,#45709,#45710,#45711,#45712,#45713,#45714,#45715,
#45716,#45717,#45718,#45719,#45720,#45721,#45722,#45723,#45724,#45725,#45726,
#45727,#45728,#45729,#45730,#45731,#45732,#45733,#45734,#45735,#45736,#45737,
#45738,#45739,#45740,#45741,#45742,#45743,#45744,#45745,#45746,#45747,#45748,
#45749,#45750,#45751,#45752,#45753,#45754,#45755,#45756,#45757,#45758,#45759,
#45760,#45761,#45762,#45763,#45764,#45765,#45766,#45767,#45768,#45769,#45770,
#45771,#45772,#45773,#45774,#45775,#45776,#45777,#45778,#45779,#45780,#45781,
#45782,#45783,#45784,#45785,#45786,#45787,#45788,#45789,#45790,#45791,#45792,
#45793,#45794,#45795,#45796,#45797,#45798,#45799,#45800,#45801,#45802,#45803,
#45804,#45805,#45806,#45807,#45808,#45809,#45810,#45811,#45812,#45813,#45814,
#45815,#45816,#45817,#45818,#45819,#45820,#45821,#45822,#45823,#45824,#45825,
#45826,#45827,#45828,#45829,#45830,#45831,#45832,#45833,#45834,#45835,#45836,
#45837,#45838,#45839,#45840,#45841,#45842,#45843,#45844,#45845,#45846,#45847,
#45848,#45849,#45850,#45851,#45852,#45853,#45854,#45855,#45856,#45857,#45858,
#45859,#45860,#45861,#45862,#45863,#45864,#45865,#45866,#45867,#45868,#45869,
#45870,#45871,#45872,#45873,#45874,#45875,#45876,#45877,#45878,#45879,#45880,
#45881,#45882,#45883,#45884,#45885,#45886,#45887,#45888,#45889,#45890,#45891,
#45892,#45893,#45894,#45895,#45896,#45897,#45898,#45899,#45900,#45901,#45902,
#45903,#45904,#45905,#45906,#45907,#45908,#45909,#45910,#45911,#45912,#45913,
#45914,#45915,#45916,#45917,#45918,#45919,#45920,#45921,#45922,#45923,#45924,
#45925,#45926,#45927,#45928,#45929,#45930,#45931,#45932,#45933,#45934,#45935,
#45936,#45937,#45938,#45939,#45940,#45941,#45942,#45943,#45944,#45945,#45946,
#45947,#45948),.UNSPECIFIED.,.F.,.F.,(4,2,2,2,2,2,2,2,2,2,2,2,2,2,2,2,2,
2,2,2,2,2,2,2,2,2,2,2,2,2,2,2,2,2,2,2,2,2,2,2,2,2,2,2,2,2,2,2,2,2,2,2,2,
2,2,2,2,2,2,2,2,2,2,2,2,2,2,2,2,2,2,2,2,2,2,2,2,2,2,2,2,2,2,2,2,2,2,2,2,
2,2,2,2,2,2,2,2,2,2,2,2,2,2,2,2,2,2,2,2,2,2,2,2,2,2,2,2,2,2,2,2,2,2,2,2,
2,2,2,2,2,2,2,2,2,2,2,2,2,2,2,4),(-2.69202105007084,-2.67637090133286,-2.65637037866237,
-2.64777232613318,-2.64643376474545,-2.64574146514728,-2.64518068180451,
-2.64461493810627,-2.64356905343837,-2.64016175042675,-2.58417962508604,
-2.49236389261529,-2.48873407707181,-2.48679243105214,-2.4855375012887,
-2.48436394594113,-2.48339573593312,-2.48237690288973,-2.48048552825973,
-2.47425903859647,-2.37060199419344,-2.32512857865517,-2.3234053116582,
-2.32263764893346,-2.3220676944243,-2.32153256847504,-2.32078766442116,
-2.31885960261658,-2.29180228064014,-2.26247520627152,-2.21160057356583,
-2.17951306019635,-2.16494208962872,-2.16257706111159,-2.16134147544218,
-2.16043211083388,-2.15944964019619,-2.15773967311286,-2.15289502066276,
-2.07862949008025,-2.03048944366382,-2.0025030824272,-2.00056034096373,
-1.99981299937901,-1.99927720455529,-1.99876461073467,-1.99803262773462,
-1.99649828049752,-1.98013761675789,-1.9603771836387,-1.85813758678381,
-1.84218690862827,-1.83956015703157,-1.83827085419179,-1.8372600867883,
-1.83613937391657,-1.83429877160718,-1.8278014284482,-1.78660207471037,
-1.73982688039598,-1.6815587408051,-1.67793942706893,-1.67686856181613,
-1.67629778421996,-1.67574279109273,-1.67507500176655,-1.6738371268906,
-1.67228700913496,-1.62187513142653,-1.54134795702907,-1.51955535959255,
-1.51667830774077,-1.51535453285432,-1.51433592340918,-1.51324269140768,
-1.51152502210243,-1.50625720071857,-1.47671042021872,-1.43252373522405,
-1.35915993022716,-1.35500585577259,-1.3538902961392,-1.35323964348548,
-1.35267886510016,-1.35200063022764,-1.35071461268247,-1.34909031512334,
-1.30950824919143,-1.25004042332307,-1.19750726677646,-1.19405203127634,
-1.19271667212103,-1.19175591929405,-1.19073733436559,-1.18939113966707,
-1.18647229515132,-1.15796750572267,-1.1340816293789,-1.06800353798191,
-1.05722705358869,-1.04973291550621,-1.0492251916827,-1.04851384707806,
-1.04626003378184,-1.044359600219,-1.03278622751438,-1.03136008722975,-1.03063766358717,
-1.03010845215822,-1.02953454985487,-1.02875979935458,-1.02699350535245,
-1.02458536933109,-1.0185552975402,-0.996419769794486,-0.945406318091502,
-0.87600117345941,-0.87146755725909,-0.869803893627545,-0.868830681569409,
-0.867918793205846,-0.86666258270707,-0.864198434959429,-0.849932637340456,
-0.831667938344258,-0.791538111422328,-0.750258920160955,-0.719205976205605,
-0.717667213459995,-0.716147696271361,-0.713413425993598,-0.709108967610019,
-0.707978475174131,-0.707324358782129,-0.706763833995119,-0.706225584158187,
-0.705132288003572,-0.700761372263859,-0.693046552444917,-0.67402532894375,
-0.6616833794075),.UNSPECIFIED.);
#257=B_SPLINE_CURVE_WITH_KNOTS('',3,(#45953,#45954,#45955,#45956,#45957,
#45958,#45959,#45960,#45961,#45962,#45963,#45964,#45965,#45966,#45967,#45968,
#45969,#45970,#45971,#45972,#45973,#45974,#45975,#45976,#45977,#45978,#45979,
#45980,#45981,#45982,#45983,#45984,#45985,#45986,#45987,#45988,#45989,#45990,
#45991,#45992,#45993,#45994,#45995,#45996,#45997,#45998,#45999,#46000,#46001,
#46002,#46003,#46004,#46005,#46006,#46007,#46008,#46009,#46010,#46011,#46012,
#46013,#46014,#46015,#46016,#46017,#46018,#46019,#46020,#46021,#46022,#46023,
#46024,#46025,#46026,#46027,#46028,#46029,#46030,#46031,#46032,#46033,#46034,
#46035,#46036,#46037,#46038,#46039,#46040,#46041,#46042,#46043,#46044,#46045,
#46046,#46047,#46048,#46049,#46050,#46051,#46052,#46053,#46054,#46055,#46056,
#46057,#46058,#46059,#46060,#46061,#46062,#46063,#46064,#46065,#46066,#46067,
#46068,#46069,#46070,#46071,#46072,#46073,#46074,#46075,#46076,#46077,#46078,
#46079,#46080,#46081,#46082,#46083,#46084,#46085,#46086,#46087,#46088,#46089,
#46090,#46091,#46092,#46093,#46094,#46095,#46096,#46097,#46098,#46099,#46100,
#46101,#46102,#46103,#46104,#46105,#46106,#46107,#46108,#46109,#46110,#46111,
#46112,#46113,#46114,#46115,#46116,#46117,#46118,#46119,#46120,#46121,#46122,
#46123,#46124,#46125,#46126,#46127,#46128,#46129,#46130,#46131,#46132,#46133,
#46134,#46135,#46136,#46137,#46138,#46139,#46140,#46141,#46142,#46143,#46144,
#46145,#46146,#46147,#46148,#46149,#46150,#46151,#46152,#46153,#46154,#46155,
#46156,#46157,#46158,#46159,#46160,#46161,#46162,#46163,#46164,#46165,#46166,
#46167,#46168,#46169,#46170,#46171,#46172,#46173,#46174,#46175,#46176,#46177,
#46178,#46179,#46180,#46181,#46182,#46183,#46184,#46185,#46186,#46187,#46188,
#46189,#46190,#46191,#46192,#46193,#46194,#46195,#46196,#46197,#46198,#46199,
#46200,#46201,#46202,#46203,#46204,#46205,#46206,#46207,#46208,#46209,#46210,
#46211,#46212,#46213,#46214,#46215,#46216,#46217,#46218,#46219,#46220,#46221,
#46222,#46223,#46224,#46225,#46226,#46227,#46228,#46229,#46230,#46231,#46232,
#46233,#46234,#46235,#46236,#46237,#46238,#46239,#46240,#46241,#46242,#46243,
#46244,#46245,#46246,#46247,#46248,#46249,#46250),.UNSPECIFIED.,.F.,.F.,
(4,2,2,2,2,2,2,2,2,2,2,2,2,2,2,2,2,2,2,2,2,2,2,2,2,2,2,2,2,2,2,2,2,2,2,
2,2,2,2,2,2,2,2,2,2,2,2,2,2,2,2,2,2,2,2,2,2,2,2,2,2,2,2,2,2,2,2,2,2,2,2,
2,2,2,2,2,2,2,2,2,2,2,2,2,2,2,2,2,2,2,2,2,2,2,2,2,2,2,2,2,2,2,2,2,2,2,2,
2,2,2,2,2,2,2,2,2,2,2,2,2,2,2,2,2,2,2,2,2,2,2,2,2,2,2,2,2,2,2,2,2,2,2,2,
2,2,2,2,2,4),(-3.40012302419576,-3.37861334262547,-3.34579899185165,-3.33610177007071,
-3.33004195076119,-3.32871108386029,-3.32746487717585,-3.32655447371831,
-3.32557735840309,-3.32418108479873,-3.32034250606838,-3.26146241461163,
-3.22320876765789,-3.19078378981384,-3.17513349868171,-3.16771973785196,
-3.16639615940618,-3.16570143700626,-3.16519434472901,-3.16464420346138,
-3.16367528205086,-3.16085796620878,-3.11308161352822,-3.05477603609166,
-3.03415185758079,-3.00895599202059,-3.00611480359512,-3.00476870275954,
-3.00375033480509,-3.00278989370851,-3.0014551386442,-2.99800240725392,
-2.94565709566628,-2.88854784681887,-2.86805022209868,-2.85231307014278,
-2.84483303039476,-2.84350668033969,-2.84281136630035,-2.8423041998841,
-2.84175433096262,-2.84078678305751,-2.83797917564052,-2.83528322908094,
-2.83312817911436,-2.83202818388997,-2.83026317398034,-2.79929098781733,
-2.72323024410347,-2.68983907210442,-2.68414918219515,-2.68238221026046,
-2.68127815831811,-2.68026349465707,-2.67896433999295,-2.67684162955999,
-2.66833575876634,-2.66627108514545,-2.66326697862997,-2.66275479712366,
-2.66065798419631,-2.65924868955021,-2.65804177490019,-2.65670792233358,
-2.65103544889531,-2.57662863793531,-2.52440097262526,-2.52123326133197,
-2.52025949593115,-2.51964277934739,-2.51907591266816,-2.51833984913381,
-2.51674219396669,-2.50480547905618,-2.50258112562136,-2.49958903003775,
-2.49828230529027,-2.49563047774737,-2.40971579781369,-2.37697100434725,
-2.36226105715761,-2.35989798772356,-2.35865299156287,-2.35765604384067,
-2.35651123194105,-2.35456207155334,-2.34783107068032,-2.24601113967426,
-2.19934920865369,-2.1976237774855,-2.19685581049498,-2.19628589478337,
-2.19575100514431,-2.19500673503428,-2.19308198898683,-2.16621472459157,
-2.0765055780489,-2.05171264319719,-2.03893917846921,-2.03665648112952,
-2.03543859090952,-2.03443397522464,-2.03326480631814,-2.03125990607609,
-2.02262118832324,-1.93087174442665,-1.88513055578382,-1.88384468416953,
-1.88234125631277,-1.8795674442905,-1.87529898367295,-1.87417209604471,
-1.87351885482268,-1.87295833295722,-1.87226959712096,-1.87094779146292,
-1.86275879724286,-1.84578604323859,-1.82120768036863,-1.72149480130843,
-1.71510902070917,-1.71319908548693,-1.71206300391871,-1.71115603126582,
-1.70994034851928,-1.70766789306571,-1.69533672190733,-1.67096468076081,
-1.58840793056682,-1.57713687452599,-1.55340688833401,-1.55153587690203,
-1.55080067290155,-1.55026819298299,-1.54969680319072,-1.54893565986218,
-1.54723524242552,-1.54494219917007,-1.52272075775901,-1.48347283921691,
-1.45229438530185,-1.39518153748121,-1.39139941994582,-1.39001175284679,
-1.38903694143529,-1.38812573059702,-1.38687383870859,-1.38443002320154,
-1.37006013660576),.UNSPECIFIED.);
#258=B_SPLINE_CURVE_WITH_KNOTS('',3,(#46252,#46253,#46254,#46255,#46256,
#46257,#46258,#46259,#46260,#46261,#46262,#46263,#46264,#46265,#46266,#46267,
#46268,#46269,#46270,#46271,#46272,#46273,#46274,#46275,#46276,#46277,#46278,
#46279,#46280,#46281,#46282,#46283,#46284,#46285,#46286,#46287,#46288,#46289,
#46290,#46291,#46292,#46293,#46294,#46295,#46296,#46297,#46298,#46299,#46300,
#46301,#46302,#46303,#46304,#46305,#46306,#46307,#46308,#46309,#46310,#46311,
#46312,#46313,#46314,#46315,#46316,#46317,#46318,#46319,#46320,#46321,#46322,
#46323,#46324,#46325,#46326,#46327,#46328,#46329,#46330,#46331,#46332,#46333,
#46334,#46335,#46336,#46337,#46338,#46339,#46340,#46341,#46342,#46343,#46344,
#46345,#46346,#46347,#46348,#46349,#46350,#46351,#46352,#46353,#46354,#46355,
#46356,#46357,#46358,#46359,#46360,#46361,#46362,#46363,#46364,#46365),
 .UNSPECIFIED.,.F.,.F.,(4,2,2,2,2,2,2,2,2,2,2,2,2,2,2,2,2,2,2,2,2,2,2,2,
2,2,2,2,2,2,2,2,2,2,2,2,2,2,2,2,2,2,2,2,2,2,2,2,2,2,2,2,2,2,2,2,4),(-0.6616833794075,
-0.633519355641761,-0.553700338753454,-0.548654798757302,-0.546915998544686,
-0.545927856781506,-0.545019944085586,-0.543796394971753,-0.541487706829025,
-0.528435400209994,-0.496753872514348,-0.488959980766652,-0.440615735169355,
-0.39615433077254,-0.394753254177924,-0.393185845516869,-0.390632909549094,
-0.389668267567501,-0.386011451872719,-0.384936331763941,-0.384364718594659,
-0.383809812505389,-0.383273501548794,-0.382607035395432,-0.380239967606707,
-0.376766082641168,-0.366833410867302,-0.33969611399129,-0.317592235843124,
-0.286335335341935,-0.229126154888774,-0.225338024910644,-0.223949348797695,
-0.222974202204585,-0.222062975147677,-0.220811522225008,-0.218370173106285,
-0.203298971359929,-0.154582171133134,-0.137981420406505,-0.129808968100797,
-0.120663247761598,-0.0831107177687953,-0.0819792174880646,-0.0808112520371773,
-0.0786142737099887,-0.0781351865346779,-0.076049215856738,-0.0640002776834103,
-0.0623982044538862,-0.0616612422995186,-0.0610941687298086,-0.0604777258993715,
-0.05984370999712,-0.0589160478804281,-0.0572784915626611,-0.000961098116046245),
 .UNSPECIFIED.);
#259=B_SPLINE_CURVE_WITH_KNOTS('',3,(#46366,#46367,#46368,#46369,#46370,
#46371,#46372,#46373,#46374,#46375,#46376,#46377,#46378,#46379,#46380,#46381,
#46382,#46383,#46384,#46385,#46386,#46387,#46388,#46389,#46390,#46391,#46392,
#46393,#46394,#46395,#46396,#46397,#46398,#46399,#46400,#46401,#46402,#46403,
#46404,#46405,#46406,#46407,#46408,#46409,#46410,#46411,#46412,#46413,#46414,
#46415,#46416,#46417,#46418,#46419,#46420,#46421,#46422,#46423,#46424,#46425,
#46426,#46427,#46428,#46429,#46430,#46431,#46432,#46433,#46434,#46435,#46436,
#46437,#46438,#46439,#46440,#46441,#46442,#46443,#46444,#46445,#46446,#46447,
#46448,#46449,#46450,#46451,#46452,#46453,#46454,#46455,#46456,#46457,#46458,
#46459,#46460,#46461,#46462,#46463,#46464,#46465,#46466,#46467,#46468,#46469,
#46470,#46471,#46472,#46473,#46474,#46475,#46476,#46477,#46478,#46479,#46480,
#46481,#46482,#46483,#46484,#46485,#46486,#46487,#46488,#46489,#46490,#46491,
#46492,#46493,#46494,#46495,#46496,#46497,#46498,#46499,#46500,#46501,#46502,
#46503,#46504,#46505,#46506,#46507,#46508,#46509,#46510,#46511,#46512,#46513,
#46514,#46515,#46516,#46517,#46518,#46519,#46520,#46521,#46522,#46523,#46524,
#46525,#46526,#46527,#46528,#46529,#46530,#46531,#46532,#46533,#46534,#46535,
#46536,#46537,#46538,#46539,#46540,#46541,#46542,#46543,#46544,#46545,#46546,
#46547,#46548,#46549,#46550,#46551,#46552,#46553,#46554,#46555,#46556,#46557,
#46558,#46559,#46560,#46561,#46562,#46563,#46564,#46565,#46566,#46567,#46568,
#46569,#46570,#46571,#46572,#46573),.UNSPECIFIED.,.F.,.F.,(4,2,2,2,2,2,
2,2,2,2,2,2,2,2,2,2,2,2,2,2,2,2,2,2,2,2,2,2,2,2,2,2,2,2,2,2,2,2,2,2,2,2,
2,2,2,2,2,2,2,2,2,2,2,2,2,2,2,2,2,2,2,2,2,2,2,2,2,2,2,2,2,2,2,2,2,2,2,2,
2,2,2,2,2,2,2,2,2,2,2,2,2,2,2,2,2,2,2,2,2,2,2,2,2,4),(-4.06158273434959,
-3.97420622812104,-3.96761257703122,-3.96459963285439,-3.96219581524972,
-3.96095248705518,-3.95994658566313,-3.95894516826372,-3.9571390927473,
-3.95159394576926,-3.86025076436609,-3.83856009378895,-3.80404285256712,
-3.80058164618932,-3.79983338456754,-3.79927056717153,-3.79869995771594,
-3.79816656668134,-3.79742763591341,-3.79593557459257,-3.7823309133433,
-3.78117891838724,-3.776240538024,-3.77317095138678,-3.74396438168119,-3.71771267133179,
-3.69067255668897,-3.65672368201556,-3.64170630826169,-3.63931231914721,
-3.63807096085153,-3.63707434586623,-3.63607409245784,-3.63427416910932,
-3.62877685704939,-3.54375756011914,-3.50416247952578,-3.47999253353542,
-3.47747584937258,-3.47679695223411,-3.47625721178888,-3.47575022767063,
-3.47519969300442,-3.47422878012438,-3.47139846478066,-3.42645777395488,
-3.37725738439123,-3.3358629998132,-3.32465482137048,-3.31787933940221,
-3.31599760187107,-3.31486784211023,-3.31385910059109,-3.31258617973585,
-3.31059517296258,-3.30240069342843,-3.29959029770863,-3.29860212401218,
-3.29815449599997,-3.29695289162195,-3.29486139561577,-3.29299577315764,
-3.29037522239285,-3.28212478639441,-3.23009736128573,-3.17871522451368,
-3.16294943826784,-3.15794390128001,-3.15479704971341,-3.15382429265853,
-3.15320781532365,-3.15264089246671,-3.15190437683198,-3.15030425577346,
-3.13830171993643,-3.13605070114259,-3.12848599246595,-3.1128587367408,
-3.05103229435915,-3.01229485671835,-2.99601000142188,-2.99356819195577,
-2.99231679785426,-2.99140573310728,-2.99043087349067,-2.98904279419967,
-2.98525745091578,-2.92440760089031,-2.83548121806865,-2.83310632575522,
-2.8313634762985,-2.83059091875818,-2.83001746616947,-2.82948782178933,
-2.82876356343905,-2.82733005470431,-2.81554215353034,-2.81471769752239,
-2.81421692335681,-2.81093890670191,-2.80845585143538,-2.79794857969055,
-2.71276901798617,-2.69260920664919),.UNSPECIFIED.);
#260=B_SPLINE_CURVE_WITH_KNOTS('',3,(#46579,#46580,#46581,#46582,#46583,
#46584,#46585,#46586,#46587,#46588,#46589,#46590,#46591,#46592,#46593,#46594,
#46595,#46596,#46597,#46598,#46599,#46600,#46601,#46602,#46603,#46604,#46605,
#46606,#46607,#46608,#46609,#46610,#46611,#46612,#46613,#46614,#46615,#46616,
#46617,#46618,#46619,#46620,#46621,#46622,#46623,#46624,#46625,#46626,#46627,
#46628,#46629,#46630,#46631,#46632,#46633,#46634,#46635,#46636,#46637,#46638,
#46639,#46640,#46641,#46642,#46643,#46644,#46645,#46646,#46647,#46648,#46649,
#46650,#46651,#46652,#46653,#46654,#46655,#46656,#46657,#46658,#46659,#46660,
#46661,#46662,#46663,#46664,#46665,#46666,#46667,#46668,#46669,#46670,#46671,
#46672,#46673,#46674,#46675,#46676,#46677,#46678,#46679,#46680,#46681,#46682,
#46683,#46684,#46685,#46686,#46687,#46688,#46689,#46690,#46691,#46692,#46693,
#46694,#46695,#46696,#46697,#46698,#46699,#46700,#46701,#46702,#46703,#46704,
#46705,#46706,#46707,#46708,#46709,#46710,#46711,#46712,#46713,#46714,#46715,
#46716,#46717,#46718,#46719,#46720),.UNSPECIFIED.,.F.,.F.,(4,3,3,3,3,3,
3,3,3,3,3,3,3,3,3,3,3,3,3,3,3,3,3,3,3,3,3,3,3,3,3,3,3,3,3,3,3,3,3,3,3,3,
3,3,3,3,3,4),(442.964564156161,443.090567200826,443.190607880541,443.283680824817,
443.376627664454,443.469476035639,443.562256540294,443.65500186245,443.747736827552,
443.840486245893,443.933334886628,444.026235327239,444.119291223324,444.190322536014,
444.28339548029,444.376342319927,444.469190691112,444.561971195768,444.654716517924,
444.747451483025,444.840200901366,444.933049542101,445.025949982713,445.119005878797,
445.190037191487,445.283110135763,445.3760569754,445.468905346585,445.56168585124,
445.654431173396,445.747166138497,445.839915556838,445.932764197574,446.025664638185,
446.118720534269,446.18975184696,446.282824791236,446.375771630873,446.468620002057,
446.561400506713,446.654145828869,446.74688079397,446.839630212311,446.932478853046,
447.025379293658,447.118435189742,447.189466502432,447.201562196418),
 .UNSPECIFIED.);
#261=B_SPLINE_CURVE_WITH_KNOTS('',3,(#46721,#46722,#46723,#46724,#46725,
#46726,#46727,#46728,#46729,#46730,#46731,#46732,#46733,#46734,#46735,#46736,
#46737,#46738,#46739,#46740,#46741,#46742,#46743,#46744,#46745,#46746,#46747,
#46748,#46749,#46750,#46751,#46752,#46753,#46754,#46755,#46756,#46757,#46758,
#46759,#46760,#46761,#46762,#46763,#46764,#46765,#46766,#46767,#46768,#46769,
#46770,#46771,#46772,#46773,#46774,#46775,#46776,#46777,#46778,#46779,#46780,
#46781,#46782,#46783,#46784,#46785,#46786,#46787,#46788,#46789,#46790,#46791,
#46792,#46793,#46794,#46795,#46796,#46797,#46798,#46799,#46800,#46801,#46802,
#46803,#46804,#46805,#46806,#46807,#46808,#46809,#46810,#46811,#46812),
 .UNSPECIFIED.,.F.,.F.,(4,2,2,2,2,2,2,2,2,2,2,2,2,2,2,2,2,2,2,2,2,2,2,2,
2,2,2,2,2,2,2,2,2,2,2,2,2,2,2,2,2,2,2,2,2,4),(-4.06137741686604,-3.99244122652865,
-3.97783305728595,-3.97576200001466,-3.97445258916643,-3.97322188765454,
-3.97231337392283,-3.97132916066007,-3.96960925355752,-3.96469234100141,
-3.88543273855108,-3.87230650744425,-3.85982632668212,-3.82739462143055,
-3.81374768679741,-3.8126935780148,-3.81200676306689,-3.81135321091697,
-3.81084922261485,-3.81027390667018,-3.8091800117638,-3.80535417760358,
-3.74350391913571,-3.716221641308,-3.68217997260114,-3.66349339697952,-3.65351999156419,
-3.65198792907096,-3.65059635891916,-3.64957051608242,-3.64862223466532,
-3.64733410810473,-3.64415627562183,-3.60945297852893,-3.56635458729749,
-3.52084856892669,-3.49327576726163,-3.48999748318605,-3.48926125500055,
-3.48857231955999,-3.48801186084446,-3.48744438482214,-3.48638946126764,
-3.48290528090794,-3.42650123911179,-3.40012302419576),.UNSPECIFIED.);
#262=B_SPLINE_CURVE_WITH_KNOTS('',3,(#46813,#46814,#46815,#46816,#46817,
#46818,#46819,#46820,#46821,#46822,#46823,#46824,#46825,#46826,#46827,#46828,
#46829,#46830,#46831,#46832,#46833,#46834,#46835,#46836,#46837,#46838,#46839,
#46840,#46841,#46842,#46843,#46844,#46845,#46846,#46847,#46848,#46849,#46850,
#46851,#46852,#46853,#46854,#46855,#46856,#46857,#46858,#46859,#46860,#46861,
#46862,#46863,#46864,#46865,#46866,#46867,#46868,#46869,#46870,#46871,#46872,
#46873,#46874,#46875,#46876,#46877,#46878,#46879,#46880,#46881,#46882,#46883,
#46884,#46885,#46886,#46887,#46888,#46889,#46890,#46891,#46892,#46893,#46894,
#46895,#46896,#46897,#46898,#46899,#46900,#46901,#46902,#46903,#46904,#46905,
#46906,#46907,#46908,#46909,#46910,#46911,#46912,#46913,#46914,#46915,#46916,
#46917,#46918,#46919,#46920,#46921,#46922,#46923,#46924,#46925,#46926,#46927,
#46928,#46929,#46930,#46931,#46932,#46933,#46934,#46935,#46936,#46937,#46938,
#46939,#46940,#46941,#46942,#46943,#46944,#46945,#46946,#46947,#46948,#46949,
#46950,#46951,#46952,#46953,#46954,#46955,#46956,#46957,#46958,#46959,#46960,
#46961,#46962,#46963,#46964,#46965,#46966,#46967,#46968,#46969,#46970,#46971,
#46972,#46973,#46974,#46975,#46976,#46977,#46978,#46979,#46980,#46981,#46982,
#46983,#46984,#46985,#46986,#46987,#46988,#46989,#46990,#46991,#46992,#46993,
#46994,#46995,#46996,#46997,#46998,#46999,#47000,#47001,#47002,#47003,#47004,
#47005,#47006,#47007,#47008,#47009,#47010,#47011,#47012,#47013,#47014,#47015,
#47016,#47017,#47018,#47019,#47020,#47021,#47022,#47023,#47024,#47025,#47026,
#47027,#47028,#47029,#47030,#47031,#47032,#47033,#47034,#47035,#47036,#47037,
#47038,#47039,#47040,#47041,#47042,#47043,#47044,#47045,#47046,#47047,#47048,
#47049,#47050,#47051,#47052,#47053,#47054,#47055,#47056,#47057,#47058,#47059,
#47060,#47061,#47062,#47063,#47064,#47065,#47066,#47067,#47068,#47069,#47070,
#47071,#47072,#47073,#47074,#47075,#47076,#47077,#47078,#47079,#47080,#47081,
#47082,#47083,#47084,#47085,#47086,#47087,#47088,#47089,#47090,#47091,#47092,
#47093,#47094,#47095,#47096,#47097,#47098,#47099,#47100,#47101,#47102,#47103,
#47104,#47105,#47106,#47107,#47108,#47109,#47110,#47111,#47112,#47113,#47114,
#47115,#47116,#47117,#47118,#47119,#47120,#47121,#47122,#47123,#47124,#47125,
#47126,#47127,#47128),.UNSPECIFIED.,.F.,.F.,(4,2,2,2,2,2,2,2,2,2,2,2,2,
2,2,2,2,2,2,2,2,2,2,2,2,2,2,2,2,2,2,2,2,2,2,2,2,2,2,2,2,2,2,2,2,2,2,2,2,
2,2,2,2,2,2,2,2,2,2,2,2,2,2,2,2,2,2,2,2,2,2,2,2,2,2,2,2,2,2,2,2,2,2,2,2,
2,2,2,2,2,2,2,2,2,2,2,2,2,2,2,2,2,2,2,2,2,2,2,2,2,2,2,2,2,2,2,2,2,2,2,2,
2,2,2,2,2,2,2,2,2,2,2,2,2,2,2,2,2,2,2,2,2,2,2,2,2,2,2,2,2,2,2,2,2,2,2,2,
4),(-2.69260920664919,-2.67763674653355,-2.67176324183407,-2.66997502699727,
-2.66886614602402,-2.66785270904156,-2.66656286434162,-2.66447142094702,
-2.65591514778885,-2.65384153972032,-2.65179951033141,-2.65117928142298,
-2.65041421580929,-2.64834048870591,-2.64676862082328,-2.64556437200839,
-2.64420939283802,-2.63871008129024,-2.62159890845879,-2.55268304811074,
-2.52875760229896,-2.51171616816116,-2.50878175250194,-2.50791027689039,
-2.50728250291302,-2.50671856254485,-2.50599176596797,-2.50448323569302,
-2.49468099198248,-2.49208949919983,-2.49105599491558,-2.48816679722052,
-2.4868950361405,-2.48462555139554,-2.40391644403388,-2.36602626955723,
-2.34994754262373,-2.34752357938152,-2.34627585393287,-2.34527858710773,
-2.3441354717486,-2.34219422737738,-2.33553506620722,-2.33172097424639,
-2.33004648135274,-2.32946397507851,-2.32802917588539,-2.3267349511877,
-2.23169726048984,-2.20970923576285,-2.18910300373577,-2.1857939642572,
-2.18480160446349,-2.18418512568023,-2.18361806169099,-2.18288117091588,
-2.18127948300773,-2.16924111125431,-2.16702118317221,-2.16562836640768,
-2.16451530608415,-2.162084280249,-2.16037042977011,-2.06564724714904,-2.03143318959107,
-2.02574908723052,-2.02392471087765,-2.02291943261526,-2.02191372626778,
-2.02067666652283,-2.01830369855196,-2.00353072834094,-1.97060579635047,
-1.86733016050763,-1.86677787999703,-1.86282896011432,-1.86173452183488,
-1.86108877483065,-1.86052752276194,-1.85982873809891,-1.85845914701179,
-1.84902827089104,-1.82459313315582,-1.72268973052317,-1.70409025305998,
-1.70134082942828,-1.70004139605516,-1.69902653009182,-1.69792227372657,
-1.69619032962716,-1.69064997161795,-1.65864456829686,-1.58099763669536,
-1.55000953999101,-1.54808380998953,-1.54021297382923,-1.53882048656305,
-1.53810752529616,-1.53754507165666,-1.53690901942732,-1.53585098150237,
-1.53213332945732,-1.44333173079549,-1.38260938618233,-1.37882414239492,
-1.37743596941246,-1.37646100284262,-1.37554980619682,-1.37429818105601,
-1.37190457230173,-1.3573768709386,-1.3251376969961,-1.25832144221263,-1.22800523221603,
-1.21737476605993,-1.21598337572553,-1.21526989229473,-1.21474300223839,
-1.21416728940651,-1.21336654376172,-1.21151792008218,-1.18917973712711,
-1.16782054189269,-1.10817219810253,-1.08575624444076,-1.07724835809942,
-1.07394024981145,-1.05790520569507,-1.05527430194043,-1.05398420173171,
-1.05297337895456,-1.05185318951687,-1.05005152804996,-1.04390313422098,
-1.03401720716491,-1.00010448362752,-0.946998185270369,-0.911513168698875,
-0.910605883831881,-0.894756765868944,-0.893029901550993,-0.892338332840257,
-0.891764757081677,-0.891173549966945,-0.890296095326423,-0.88795936487484,
-0.829349700561649,-0.790619811328917,-0.736408991355979,-0.7328812553212,
-0.731534035486197,-0.730570157917393,-0.729654904793902,-0.728374727961411,
-0.725844741972436,-0.706222593187417,-0.675377349731977,-0.662344877873636),
 .UNSPECIFIED.);
#263=B_SPLINE_CURVE_WITH_KNOTS('',3,(#47134,#47135,#47136,#47137,#47138,
#47139,#47140,#47141),.UNSPECIFIED.,.F.,.F.,(4,1,1,1,1,4),(449.247756666875,
450.188610468851,451.188325124324,452.188039779797,453.187754435269,453.485536920593),
 .UNSPECIFIED.);
#264=B_SPLINE_CURVE_WITH_KNOTS('',3,(#47142,#47143,#47144,#47145,#47146,
#47147,#47148,#47149,#47150,#47151,#47152,#47153,#47154,#47155,#47156,#47157,
#47158,#47159,#47160,#47161,#47162,#47163,#47164,#47165,#47166,#47167,#47168,
#47169,#47170,#47171,#47172,#47173,#47174,#47175,#47176,#47177,#47178,#47179,
#47180,#47181,#47182,#47183,#47184,#47185,#47186,#47187,#47188,#47189,#47190,
#47191,#47192,#47193,#47194,#47195,#47196,#47197,#47198,#47199,#47200,#47201,
#47202,#47203,#47204,#47205,#47206,#47207,#47208,#47209,#47210,#47211),
 .UNSPECIFIED.,.F.,.F.,(4,3,3,3,3,3,3,3,3,3,3,3,3,3,3,3,3,3,3,3,3,3,3,4),
(447.201562196418,447.294617197158,447.387549689525,447.480387294148,447.573161825754,
447.665904400597,447.75863984103,447.851392956841,447.94424706055,448.03715586022,
448.130216493826,448.189181157905,448.282254102181,448.375200941818,448.468049313003,
448.560829817658,448.653575139815,448.746310104916,448.839059523257,448.931908163992,
449.024808604604,449.117864500688,449.188895813378,449.247749463341),
 .UNSPECIFIED.);
#265=B_SPLINE_CURVE_WITH_KNOTS('',3,(#47213,#47214,#47215,#47216,#47217,
#47218,#47219,#47220,#47221,#47222,#47223,#47224,#47225,#47226,#47227,#47228,
#47229,#47230,#47231,#47232,#47233,#47234,#47235,#47236,#47237,#47238,#47239,
#47240,#47241,#47242,#47243,#47244,#47245,#47246,#47247,#47248,#47249,#47250,
#47251,#47252,#47253,#47254,#47255,#47256,#47257,#47258,#47259,#47260,#47261,
#47262,#47263,#47264,#47265,#47266,#47267,#47268,#47269,#47270,#47271,#47272,
#47273,#47274,#47275,#47276,#47277,#47278,#47279,#47280,#47281,#47282,#47283,
#47284,#47285,#47286,#47287,#47288,#47289,#47290,#47291,#47292,#47293,#47294,
#47295,#47296,#47297,#47298,#47299,#47300,#47301,#47302,#47303,#47304,#47305,
#47306,#47307,#47308,#47309,#47310),.UNSPECIFIED.,.F.,.F.,(4,2,2,2,2,2,
2,2,2,2,2,2,2,2,2,2,2,2,2,2,2,2,2,2,2,2,2,2,2,2,2,2,2,2,2,2,2,2,2,2,2,2,
2,2,2,2,2,2,4),(-0.662344877873636,-0.634147804424907,-0.580833096738116,
-0.579501825629761,-0.57793739142578,-0.575409913535667,-0.574376360467817,
-0.57075434030301,-0.569683207783907,-0.569112400137223,-0.568557448608283,
-0.567876046496436,-0.567150355838213,-0.564025633865396,-0.534619709700243,
-0.48611105310166,-0.414665807901001,-0.411359875691538,-0.409358109351963,
-0.408081752476541,-0.407072501748034,-0.40594448752745,-0.404778786662001,
-0.403049163865885,-0.386425478526341,-0.346370971119457,-0.318766618052582,
-0.251801668323609,-0.247851111192788,-0.246756581152906,-0.246110859141434,
-0.245549679194623,-0.244851049071112,-0.244101387738018,-0.242897603552263,
-0.22898075842022,-0.194229241459736,-0.180761196698222,-0.166723996205132,
-0.0922711416211886,-0.0874323107877999,-0.085723351157587,-0.084741187830486,
-0.0838319376635584,-0.0825962488813401,-0.0812799986883665,-0.0791929123388455,
-0.0646429522359529,-0.0009614827507557),.UNSPECIFIED.);
#266=B_SPLINE_CURVE_WITH_KNOTS('',3,(#47311,#47312,#47313,#47314,#47315,
#47316,#47317,#47318,#47319,#47320,#47321,#47322,#47323,#47324,#47325,#47326,
#47327,#47328,#47329,#47330,#47331,#47332,#47333,#47334,#47335,#47336,#47337,
#47338,#47339,#47340,#47341,#47342,#47343,#47344,#47345,#47346,#47347,#47348,
#47349,#47350,#47351,#47352,#47353,#47354,#47355,#47356,#47357,#47358,#47359,
#47360,#47361,#47362,#47363,#47364,#47365,#47366,#47367,#47368,#47369,#47370,
#47371,#47372,#47373,#47374,#47375,#47376,#47377,#47378,#47379,#47380,#47381,
#47382,#47383,#47384,#47385,#47386,#47387,#47388,#47389,#47390,#47391,#47392,
#47393,#47394,#47395,#47396,#47397,#47398,#47399,#47400,#47401,#47402,#47403,
#47404,#47405,#47406,#47407,#47408,#47409,#47410,#47411,#47412,#47413,#47414,
#47415,#47416,#47417,#47418,#47419,#47420,#47421,#47422,#47423,#47424,#47425,
#47426,#47427,#47428,#47429,#47430,#47431,#47432,#47433,#47434,#47435,#47436,
#47437,#47438,#47439,#47440,#47441,#47442,#47443,#47444,#47445,#47446,#47447,
#47448,#47449,#47450,#47451,#47452,#47453,#47454,#47455,#47456,#47457,#47458,
#47459,#47460,#47461,#47462,#47463,#47464,#47465,#47466,#47467,#47468,#47469,
#47470,#47471,#47472,#47473,#47474,#47475,#47476,#47477,#47478,#47479,#47480,
#47481,#47482,#47483,#47484,#47485,#47486,#47487,#47488,#47489,#47490,#47491,
#47492,#47493,#47494,#47495,#47496,#47497,#47498,#47499,#47500,#47501,#47502,
#47503,#47504,#47505,#47506),.UNSPECIFIED.,.F.,.F.,(4,2,2,2,2,2,2,2,2,2,
2,2,2,2,2,2,2,2,2,2,2,2,2,2,2,2,2,2,2,2,2,2,2,2,2,2,2,2,2,2,2,2,2,2,2,2,
2,2,2,2,2,2,2,2,2,2,2,2,2,2,2,2,2,2,2,2,2,2,2,2,2,2,2,2,2,2,2,2,2,2,2,2,
2,2,2,2,2,2,2,2,2,2,2,2,2,2,2,4),(-4.06034582511648,-3.99445104399732,-3.9852077296334,
-3.98403038375232,-3.98329179980511,-3.98260114528172,-3.9820405063354,
-3.98138876972932,-3.98026839366226,-3.97606571068478,-3.90531020465583,
-3.89193171359876,-3.87882062793399,-3.84018575303294,-3.82511646498073,
-3.82341085472919,-3.82225519304645,-3.82113421344775,-3.82012358057946,
-3.8188349654214,-3.81621140624214,-3.80032149281129,-3.79913113519368,
-3.79791814480669,-3.7965260135535,-3.79042953041537,-3.74282049438889,
-3.71746008945393,-3.69060442945423,-3.67037832085652,-3.66465286922078,
-3.66116367131339,-3.66041322675799,-3.65971404865467,-3.65915285791271,
-3.65850760070165,-3.65741496289121,-3.65348196872246,-3.58638920721675,
-3.53832647296154,-3.50731664735932,-3.50114898008441,-3.49981117853225,
-3.49855992756465,-3.49764878688548,-3.49667367546273,-3.49528495217581,
-3.49149610080983,-3.42982922814949,-3.3947579156103,-3.36142725529963,
-3.34660045227513,-3.34141186054972,-3.33817611134175,-3.33744254027057,
-3.33675549489367,-3.33619506909819,-3.33562632917131,-3.33456534674392,
-3.33103043557557,-3.27352017837254,-3.2247167536341,-3.19766910855078,
-3.17945186096262,-3.17696967049981,-3.17569614944256,-3.17478192134963,
-3.17381568673515,-3.17245958834097,-3.16887623835524,-3.11411314341179,
-3.05930644977589,-3.03868505862885,-3.02319418247306,-3.0158090537654,
-3.01452621991955,-3.01384016723687,-3.01333397662759,-3.01277938234999,
-3.01178855538521,-3.00881240037603,-2.95992484481501,-2.89573188099968,
-2.88183452553617,-2.85745824304657,-2.85437088914118,-2.85297736317385,
-2.85195109045097,-2.85100312665893,-2.84971652378462,-2.84719941705113,
-2.82746988099277,-2.82240507141891,-2.80186097571615,-2.72952413268572,
-2.70315217311971,-2.6930409546565,-2.69200921985429),.UNSPECIFIED.);
#267=B_SPLINE_CURVE_WITH_KNOTS('',3,(#47512,#47513,#47514,#47515,#47516,
#47517,#47518,#47519,#47520,#47521,#47522,#47523,#47524,#47525,#47526,#47527,
#47528,#47529,#47530,#47531,#47532,#47533,#47534,#47535,#47536,#47537,#47538,
#47539,#47540,#47541,#47542,#47543,#47544,#47545,#47546,#47547,#47548,#47549,
#47550,#47551,#47552,#47553,#47554,#47555,#47556,#47557,#47558,#47559,#47560,
#47561,#47562,#47563,#47564,#47565,#47566,#47567,#47568,#47569,#47570,#47571,
#47572,#47573,#47574,#47575,#47576,#47577,#47578,#47579,#47580,#47581,#47582,
#47583,#47584,#47585,#47586,#47587,#47588,#47589,#47590,#47591,#47592,#47593,
#47594,#47595,#47596,#47597,#47598,#47599,#47600,#47601,#47602,#47603,#47604,
#47605,#47606,#47607,#47608,#47609,#47610,#47611,#47612,#47613,#47614,#47615,
#47616,#47617,#47618,#47619,#47620,#47621,#47622,#47623,#47624,#47625,#47626,
#47627,#47628,#47629,#47630,#47631,#47632,#47633,#47634,#47635,#47636,#47637,
#47638,#47639,#47640,#47641,#47642,#47643,#47644,#47645,#47646,#47647,#47648,
#47649,#47650,#47651,#47652,#47653,#47654,#47655,#47656,#47657,#47658,#47659,
#47660,#47661,#47662,#47663,#47664,#47665,#47666,#47667,#47668,#47669,#47670,
#47671,#47672,#47673,#47674,#47675,#47676,#47677,#47678,#47679,#47680,#47681,
#47682,#47683,#47684,#47685,#47686,#47687,#47688,#47689,#47690,#47691,#47692,
#47693,#47694,#47695,#47696,#47697,#47698,#47699,#47700,#47701,#47702,#47703,
#47704,#47705,#47706,#47707,#47708,#47709,#47710,#47711,#47712,#47713,#47714,
#47715,#47716,#47717,#47718,#47719,#47720,#47721,#47722,#47723,#47724,#47725,
#47726,#47727,#47728,#47729,#47730,#47731,#47732,#47733,#47734,#47735,#47736,
#47737),.UNSPECIFIED.,.F.,.F.,(4,2,2,2,2,2,2,2,2,2,2,2,2,2,2,2,2,2,2,2,
2,2,2,2,2,2,2,2,2,2,2,2,2,2,2,2,2,2,2,2,2,2,2,2,2,2,2,2,2,2,2,2,2,2,2,2,
2,2,2,2,2,2,2,2,2,2,2,2,2,2,2,2,2,2,2,2,2,2,2,2,2,2,2,2,2,2,2,2,2,2,2,2,
2,2,2,2,2,2,2,2,2,2,2,2,2,2,2,2,2,2,2,2,4),(-1.37005249657453,-1.34947742657622,
-1.34606802935087,-1.34474042282689,-1.34378184118414,-1.3428150238564,
-1.34151935588637,-1.33883083194066,-1.33533913332211,-1.3060739226842,
-1.24370437695282,-1.18739402378087,-1.18392903894686,-1.18287633209735,
-1.18230926608889,-1.18174870665093,-1.18105891401461,-1.17973201011291,
-1.17141942514509,-1.15310303345706,-1.12795810155243,-1.04050191887311,
-1.03843372157579,-1.02498010866747,-1.02273937652417,-1.02140514142119,
-1.02038496355219,-1.01931834570073,-1.01775811421082,-1.01321564832487,
-1.00650593044383,-0.987171779782808,-0.935326323447163,-0.878303078665348,
-0.875250910405159,-0.873767488080319,-0.871404444155965,-0.869351236206721,
-0.861560025770046,-0.8601722176098,-0.859460340846227,-0.858898082677647,
-0.858261537691823,-0.85717932823904,-0.852955908365347,-0.82145192471196,
-0.737718877608971,-0.721308065905467,-0.718017355768539,-0.715913176560136,
-0.715428920456607,-0.711650108398861,-0.707916802208063,-0.70110522376816,
-0.699147113526778,-0.698000293069543,-0.697003558202362,-0.695786298577297,
-0.693480028775742,-0.690584024033379,-0.684332867718261,-0.666745044899952,
-0.625891942391485,-0.550172923607249,-0.538841001798487,-0.537266785476882,
-0.536535150672556,-0.535968941154943,-0.535350081477446,-0.534346848098215,
-0.530937230737147,-0.509293406041016,-0.48468382235598,-0.477431376513894,
-0.471256915294787,-0.465899268150126,-0.419827025605223,-0.403252692531126,
-0.400738152790972,-0.37969749135209,-0.376885145738053,-0.375553533517467,
-0.374533743684087,-0.373592365508861,-0.372523950765309,-0.369522007840247,
-0.365550490408535,-0.355993501683274,-0.324036484670031,-0.307980280253675,
-0.2200381163081,-0.215762052327458,-0.214272243730014,-0.213549111289099,
-0.212985560230024,-0.212355627141011,-0.211303259550368,-0.207408163838918,
-0.118889757535656,-0.103732932298317,-0.0979144688668333,-0.0840904985382303,
-0.0756962699386087,-0.0723811977320567,-0.0562807987276871,-0.053646672577637,
-0.0523559451565651,-0.0513450680913494,-0.0504022073920895,-0.0493040090954308,
-0.0477372101345243,-0.045047651856617,-0.000960743384126951),
 .UNSPECIFIED.);
#268=B_SPLINE_CURVE_WITH_KNOTS('',3,(#47738,#47739,#47740,#47741,#47742,
#47743),.UNSPECIFIED.,.F.,.F.,(4,1,1,4),(453.485536920593,454.187469090742,
455.187183746215,455.530927222854),.UNSPECIFIED.);
#269=B_SPLINE_CURVE_WITH_KNOTS('',3,(#47744,#47745,#47746,#47747,#47748,
#47749,#47750,#47751,#47752,#47753,#47754,#47755,#47756,#47757,#47758,#47759,
#47760,#47761,#47762,#47763,#47764,#47765,#47766,#47767,#47768,#47769,#47770,
#47771,#47772,#47773,#47774,#47775,#47776,#47777,#47778,#47779,#47780,#47781,
#47782,#47783,#47784,#47785,#47786,#47787,#47788,#47789,#47790,#47791,#47792,
#47793,#47794,#47795,#47796,#47797,#47798,#47799,#47800,#47801,#47802,#47803,
#47804,#47805,#47806,#47807,#47808,#47809,#47810,#47811,#47812,#47813,#47814,
#47815,#47816,#47817,#47818,#47819,#47820,#47821,#47822,#47823,#47824,#47825,
#47826,#47827,#47828,#47829,#47830,#47831,#47832,#47833,#47834,#47835,#47836,
#47837,#47838,#47839,#47840,#47841,#47842,#47843,#47844,#47845,#47846,#47847,
#47848,#47849,#47850,#47851,#47852,#47853,#47854,#47855,#47856,#47857,#47858,
#47859,#47860,#47861,#47862,#47863,#47864,#47865,#47866,#47867,#47868,#47869,
#47870,#47871,#47872,#47873,#47874,#47875,#47876,#47877,#47878,#47879,#47880,
#47881,#47882,#47883,#47884,#47885,#47886,#47887,#47888,#47889,#47890,#47891,
#47892,#47893,#47894,#47895,#47896,#47897,#47898,#47899,#47900,#47901,#47902,
#47903,#47904,#47905,#47906,#47907,#47908,#47909,#47910,#47911,#47912,#47913,
#47914,#47915,#47916,#47917,#47918,#47919,#47920,#47921,#47922,#47923,#47924,
#47925,#47926,#47927,#47928,#47929,#47930,#47931,#47932,#47933,#47934,#47935,
#47936,#47937,#47938,#47939,#47940,#47941,#47942,#47943,#47944,#47945,#47946,
#47947,#47948,#47949,#47950,#47951,#47952,#47953,#47954,#47955,#47956,#47957,
#47958,#47959,#47960,#47961,#47962,#47963,#47964,#47965,#47966,#47967,#47968,
#47969,#47970,#47971,#47972,#47973,#47974,#47975,#47976,#47977,#47978,#47979,
#47980,#47981,#47982,#47983,#47984,#47985,#47986,#47987,#47988,#47989,#47990,
#47991,#47992,#47993,#47994,#47995,#47996,#47997,#47998,#47999,#48000,#48001,
#48002,#48003,#48004,#48005,#48006,#48007,#48008,#48009,#48010,#48011,#48012,
#48013),.UNSPECIFIED.,.F.,.F.,(4,2,2,2,2,2,2,2,2,2,2,2,2,2,2,2,2,2,2,2,
2,2,2,2,2,2,2,2,2,2,2,2,2,2,2,2,2,2,2,2,2,2,2,2,2,2,2,2,2,2,2,2,2,2,2,2,
2,2,2,2,2,2,2,2,2,2,2,2,2,2,2,2,2,2,2,2,2,2,2,2,2,2,2,2,2,2,2,2,2,2,2,2,
2,2,2,2,2,2,2,2,2,2,2,2,2,2,2,2,2,2,2,2,2,2,2,2,2,2,2,2,2,2,2,2,2,2,2,2,
2,2,2,2,2,2,4),(-2.69200921985429,-2.69165321726174,-2.69094492855103,-2.69043602228833,
-2.68989173778862,-2.68911289351126,-2.68696659719547,-2.65386039208112,
-2.58216715875224,-2.53909144951289,-2.5347021149539,-2.53146748021361,
-2.53006771374992,-2.52903514301789,-2.52809474322263,-2.5268383893358,
-2.52377637728473,-2.49480666964021,-2.40388668536287,-2.39339612428702,
-2.37261064295925,-2.36929745269862,-2.36829632460508,-2.36767785309433,
-2.36711136523722,-2.36637850861288,-2.36479834071029,-2.35332202431041,
-2.35001553946594,-2.25876051509073,-2.22950881806805,-2.21046852014313,
-2.20794641268655,-2.20667833707885,-2.20576486098085,-2.20479649551643,
-2.20343262027594,-2.20060762028636,-2.17026987433493,-2.15993609144862,
-2.08376853296493,-2.04768000709782,-2.0457860202543,-2.04498816166278,
-2.04441295433481,-2.04388539197335,-2.04316935936716,-2.04176815597483,
-2.03088139231954,-2.00015673704151,-1.89231080395764,-1.88618497250253,
-1.88430574483263,-1.88328942155656,-1.88228476780398,-1.88106651957949,
-1.87878222896055,-1.86597725092406,-1.84118862290925,-1.75132733423306,
-1.72457965587552,-1.7226567568446,-1.72191276475521,-1.72137792715382,
-1.72080792251254,-1.72003959242045,-1.71831233261279,-1.67074170691629,
-1.56899289622534,-1.56298881875898,-1.5611243857828,-1.56011105215202,
-1.55910618972366,-1.55790771252357,-1.55568457569179,-1.55291786275152,
-1.49383231944649,-1.42461989541395,-1.40427278527274,-1.40014892190999,
-1.39903652947395,-1.39838667546102,-1.39788202393566,-1.39721416841314,
-1.39599002547766,-1.38977804068478,-1.37738240180472,-1.35388154729539,
-1.249132390923,-1.24040456449739,-1.23847166115012,-1.23721680900121,-1.23620985098609,
-1.23509181032965,-1.23327109109389,-1.23107158491522,-1.2267647527842,
-1.18509966529055,-1.1327460959081,-1.08701879002559,-1.0857060874427,-1.08418438433995,
-1.08150988702066,-1.07715400133105,-1.07601867342492,-1.07536354798018,
-1.07480325559912,-1.07411710724616,-1.07280719997668,-1.06489171719722,
-1.05176581656063,-1.02524132766951,-0.946818656505899,-0.918992858982936,
-0.915922201012758,-0.914685432211556,-0.913656341989606,-0.912710674531701,
-0.911285265281233,-0.907903263444656,-0.903264508743662,-0.89148934009968,
-0.865710076516489,-0.825415060322478,-0.766528317792936,-0.754991821724399,
-0.753409752631514,-0.752676686519284,-0.752110326950788,-0.751492296094884,
-0.750492521751862,-0.747114141450464,-0.725793593103464,-0.681591163627844,
-0.661698739247463),.UNSPECIFIED.);
#270=B_SPLINE_CURVE_WITH_KNOTS('',3,(#48018,#48019,#48020,#48021,#48022,
#48023,#48024,#48025,#48026,#48027,#48028,#48029,#48030,#48031,#48032,#48033,
#48034,#48035,#48036,#48037,#48038,#48039,#48040,#48041,#48042,#48043,#48044,
#48045,#48046,#48047,#48048,#48049,#48050,#48051,#48052,#48053,#48054,#48055,
#48056,#48057,#48058,#48059,#48060,#48061,#48062,#48063,#48064,#48065,#48066,
#48067,#48068,#48069,#48070,#48071,#48072,#48073,#48074,#48075,#48076,#48077,
#48078,#48079,#48080,#48081,#48082,#48083,#48084,#48085,#48086,#48087,#48088,
#48089,#48090,#48091,#48092,#48093,#48094,#48095,#48096,#48097,#48098,#48099,
#48100,#48101,#48102,#48103,#48104,#48105,#48106,#48107,#48108,#48109,#48110,
#48111,#48112,#48113,#48114,#48115,#48116,#48117,#48118,#48119,#48120,#48121,
#48122,#48123,#48124,#48125,#48126,#48127,#48128,#48129,#48130,#48131,#48132,
#48133,#48134,#48135,#48136,#48137,#48138,#48139,#48140,#48141,#48142,#48143,
#48144,#48145,#48146,#48147,#48148,#48149,#48150,#48151,#48152,#48153,#48154,
#48155,#48156,#48157,#48158,#48159,#48160,#48161,#48162,#48163,#48164,#48165,
#48166,#48167,#48168,#48169,#48170,#48171,#48172,#48173,#48174,#48175,#48176,
#48177,#48178,#48179,#48180,#48181,#48182,#48183,#48184,#48185,#48186,#48187,
#48188,#48189,#48190,#48191,#48192,#48193,#48194,#48195,#48196,#48197,#48198,
#48199,#48200,#48201,#48202,#48203,#48204,#48205,#48206,#48207,#48208,#48209,
#48210,#48211,#48212,#48213,#48214,#48215,#48216,#48217,#48218,#48219,#48220,
#48221,#48222,#48223,#48224,#48225,#48226,#48227,#48228,#48229,#48230,#48231,
#48232,#48233,#48234,#48235,#48236,#48237,#48238,#48239,#48240,#48241,#48242,
#48243,#48244,#48245,#48246,#48247,#48248,#48249,#48250,#48251,#48252,#48253,
#48254,#48255,#48256,#48257,#48258,#48259,#48260,#48261,#48262,#48263,#48264,
#48265,#48266,#48267,#48268,#48269,#48270,#48271,#48272,#48273,#48274,#48275,
#48276,#48277,#48278,#48279,#48280,#48281,#48282,#48283,#48284,#48285,#48286,
#48287,#48288,#48289,#48290,#48291,#48292,#48293,#48294,#48295,#48296,#48297,
#48298,#48299,#48300,#48301,#48302,#48303,#48304,#48305,#48306,#48307,#48308,
#48309,#48310,#48311,#48312,#48313,#48314,#48315,#48316,#48317,#48318,#48319,
#48320,#48321,#48322,#48323,#48324,#48325,#48326,#48327,#48328,#48329,#48330,
#48331,#48332,#48333,#48334,#48335,#48336,#48337,#48338,#48339),
 .UNSPECIFIED.,.F.,.F.,(4,2,2,2,2,2,2,2,2,2,2,2,2,2,2,2,2,2,2,2,2,2,2,2,
2,2,2,2,2,2,2,2,2,2,2,2,2,2,2,2,2,2,2,2,2,2,2,2,2,2,2,2,2,2,2,2,2,2,2,2,
2,2,2,2,2,2,2,2,2,2,2,2,2,2,2,2,2,2,2,2,2,2,2,2,2,2,2,2,2,2,2,2,2,2,2,2,
2,2,2,2,2,2,2,2,2,2,2,2,2,2,2,2,2,2,2,2,2,2,2,2,2,2,2,2,2,2,2,2,2,2,2,2,
2,2,2,2,2,2,2,2,2,2,2,2,2,2,2,2,2,2,2,2,2,2,2,2,2,2,2,2,4),(-3.40020803169445,
-3.35398570630315,-3.29013598947784,-3.28471453628915,-3.2829927101431,
-3.2818987238525,-3.28088073172867,-3.27955963004755,-3.27669578807702,
-3.26875965935094,-3.26642402437193,-3.26563970565285,-3.2640494092677,
-3.26345428659867,-3.2613705723809,-3.25988002549393,-3.25867461756904,
-3.25735496832278,-3.25121029429168,-3.16052920749821,-3.13420323739372,
-3.12646157331662,-3.12356779444746,-3.12216665504375,-3.12133511339737,
-3.12061412057079,-3.12005234574844,-3.11952264061871,-3.1187980366879,
-3.11736305085652,-3.10552991326149,-3.10474106284485,-3.10427868228702,
-3.10336680774234,-3.10300764822804,-3.02159881000798,-2.98002503432068,
-2.96300453254703,-2.96054706496354,-2.9592924114776,-2.95838090468532,
-2.95740739439603,-2.95574146390953,-2.95119144571076,-2.87770004397311,
-2.82219124676294,-2.80210250940144,-2.79994180147395,-2.79880992330032,
-2.79785040550319,-2.79724658336112,-2.79667953399562,-2.79594238529268,
-2.79433905002222,-2.78225339741649,-2.78100941024525,-2.77864282286437,
-2.7772112825547,-2.74661315305248,-2.67621596014387,-2.64429393188747,
-2.63874000431064,-2.63700241192106,-2.63590485381464,-2.63488799813024,
-2.63357464424756,-2.63075209409682,-2.62275996417313,-2.62090398579852,
-2.61897589381954,-2.61819339237392,-2.61748186929377,-2.61540608505668,
-2.61450914757871,-2.61045109072549,-2.60840357286315,-2.59613601351232,
-2.52087870550378,-2.4965222512257,-2.47885259714141,-2.47684851220761,
-2.47577661299671,-2.47508230041829,-2.47445948346121,-2.47391039702322,
-2.47324873384539,-2.47208539630559,-2.46727602544291,-2.37043576878027,
-2.35211470484474,-2.32857141440818,-2.31662110282314,-2.31438070669267,
-2.31317191075265,-2.312265585865,-2.3111244023118,-2.3091916117794,-2.30260670372054,
-2.29875568237016,-2.29480499064254,-2.29273362907647,-2.29098857853584,
-2.28977151563447,-2.28754665537073,-2.283254116112,-2.20645379036111,-2.15407249799104,
-2.15233768703452,-2.15156803611938,-2.15099786563572,-2.15046348525701,
-2.14972106161175,-2.14780728535993,-2.12161250245554,-2.03136322932114,
-1.99518731497887,-1.99197842230844,-1.99068493155661,-1.98973529863622,
-1.9887104799783,-1.98732468840064,-1.98419058145667,-1.93429768311864,
-1.83989692624847,-1.83858202211452,-1.83705663898469,-1.83455798955058,
-1.8335118803677,-1.82987556844279,-1.8288028172068,-1.82823169499027,-1.82767678252558,
-1.82699591944879,-1.82571132828652,-1.81835395861684,-1.80294688438215,
-1.78979566029935,-1.70646181409129,-1.69248356428609,-1.67146520918019,
-1.66861722691605,-1.66729901650909,-1.66628137167775,-1.66520797260919,
-1.66353771887348,-1.66158690583593,-1.65793330710152,-1.6263682433561,
-1.58074957163203,-1.55120522810682,-1.50931439754957,-1.50666690459669,
-1.50572235870822,-1.5051770655646,-1.50466854905917,-1.50396285739634,
-1.50255925117531,-1.49208045462941,-1.46417818883468,-1.39796080861194,
-1.37005249657453),.UNSPECIFIED.);
#271=B_SPLINE_CURVE_WITH_KNOTS('',3,(#48341,#48342,#48343,#48344,#48345,
#48346,#48347,#48348,#48349,#48350,#48351,#48352,#48353,#48354,#48355,#48356,
#48357,#48358,#48359,#48360,#48361,#48362,#48363,#48364,#48365,#48366,#48367,
#48368,#48369,#48370,#48371,#48372,#48373,#48374,#48375,#48376,#48377,#48378,
#48379,#48380,#48381,#48382,#48383,#48384,#48385,#48386,#48387,#48388,#48389,
#48390,#48391,#48392,#48393,#48394,#48395,#48396,#48397,#48398,#48399,#48400,
#48401,#48402,#48403,#48404,#48405,#48406,#48407,#48408,#48409,#48410,#48411,
#48412,#48413,#48414,#48415,#48416,#48417,#48418,#48419,#48420,#48421,#48422,
#48423,#48424,#48425,#48426,#48427,#48428,#48429,#48430,#48431,#48432,#48433,
#48434),.UNSPECIFIED.,.F.,.F.,(4,2,2,2,2,2,2,2,2,2,2,2,2,2,2,2,2,2,2,2,
2,2,2,2,2,2,2,2,2,2,2,2,2,2,2,2,2,2,2,2,2,2,2,2,2,2,4),(-0.661698739247463,
-0.63155827478073,-0.596440654951037,-0.593254201436511,-0.59196463836349,
-0.591016042432585,-0.590055886256616,-0.589058467814166,-0.586771017828778,
-0.573748051955903,-0.549672423321915,-0.51894174027973,-0.442624554119548,
-0.432068640809763,-0.43068029678856,-0.429967659942444,-0.429441044648925,
-0.428865271497753,-0.428063804292975,-0.426148043269977,-0.423510346780509,
-0.395101611831078,-0.357958254519825,-0.339759849144639,-0.315622408306712,
-0.299752363421774,-0.292937832283236,-0.291438612422854,-0.272844813936617,
-0.270095870077907,-0.268796622041962,-0.267781882656786,-0.266840258423881,
-0.265757452267252,-0.262689961811862,-0.229166499655505,-0.208869859261655,
-0.113498928485787,-0.108564664346256,-0.107481722724927,-0.106781224964328,
-0.106219892526339,-0.105575491922326,-0.104458328543778,-0.0998185169514192,
-0.0603751173097801,-0.000962380706964255),.UNSPECIFIED.);
#272=B_SPLINE_CURVE_WITH_KNOTS('',3,(#48435,#48436,#48437,#48438,#48439,
#48440,#48441,#48442,#48443,#48444,#48445,#48446,#48447,#48448,#48449,#48450,
#48451,#48452,#48453,#48454,#48455,#48456,#48457,#48458,#48459,#48460,#48461,
#48462,#48463,#48464,#48465,#48466,#48467,#48468,#48469,#48470,#48471,#48472,
#48473,#48474,#48475,#48476,#48477,#48478,#48479,#48480,#48481,#48482,#48483,
#48484,#48485,#48486,#48487,#48488,#48489,#48490,#48491,#48492,#48493,#48494,
#48495,#48496,#48497,#48498,#48499,#48500,#48501,#48502,#48503,#48504,#48505,
#48506,#48507,#48508,#48509,#48510,#48511,#48512,#48513,#48514,#48515,#48516,
#48517,#48518,#48519,#48520,#48521,#48522,#48523,#48524,#48525,#48526,#48527,
#48528,#48529,#48530,#48531,#48532,#48533,#48534,#48535,#48536,#48537,#48538,
#48539,#48540,#48541,#48542,#48543,#48544,#48545,#48546,#48547,#48548,#48549,
#48550,#48551,#48552,#48553,#48554,#48555,#48556,#48557,#48558,#48559,#48560,
#48561,#48562,#48563,#48564,#48565,#48566,#48567,#48568,#48569,#48570,#48571,
#48572,#48573,#48574,#48575,#48576),.UNSPECIFIED.,.F.,.F.,(4,3,3,3,3,3,
3,3,3,3,3,3,3,3,3,3,3,3,3,3,3,3,3,3,3,3,3,3,3,3,3,3,3,3,3,3,3,3,3,3,3,3,
3,3,3,3,3,4),(461.814120077699,461.906710520206,461.999282389779,462.091860611502,
462.184470108962,462.277191924903,462.369980696409,462.462916807322,462.486523846003,
462.579596790279,462.672543629916,462.765392001101,462.858172505756,462.950917827912,
463.043652793014,463.136402211355,463.22925085209,463.322151292702,463.415207188786,
463.486238501476,463.579311445752,463.672258285389,463.765106656574,463.857887161229,
463.950632483385,464.043367448486,464.136116866827,464.228965507563,464.321865948174,
464.414921844258,464.485953156949,464.579026101225,464.671972940862,464.764821312047,
464.857601816702,464.950347138859,465.04308210396,465.135831522301,465.228680163036,
465.321580603648,465.414636499732,465.485667812422,465.578733049488,465.671678204188,
465.766469833072,465.859244858906,465.955044789315,466.050844719725),
 .UNSPECIFIED.);
#273=B_SPLINE_CURVE_WITH_KNOTS('',3,(#48582,#48583,#48584,#48585,#48586,
#48587,#48588,#48589,#48590),.UNSPECIFIED.,.F.,.F.,(4,1,1,1,1,1,4),(468.097305384879,
468.183474267362,469.183188922835,470.182903578308,471.18261823378,472.182332889253,
472.335020342325),.UNSPECIFIED.);
#274=B_SPLINE_CURVE_WITH_KNOTS('',3,(#48591,#48592,#48593,#48594,#48595,
#48596,#48597,#48598,#48599,#48600,#48601,#48602,#48603,#48604,#48605,#48606,
#48607,#48608,#48609,#48610,#48611,#48612,#48613,#48614,#48615,#48616,#48617,
#48618,#48619,#48620,#48621,#48622,#48623,#48624,#48625,#48626,#48627,#48628,
#48629,#48630,#48631,#48632,#48633,#48634,#48635,#48636,#48637,#48638,#48639,
#48640,#48641,#48642,#48643,#48644,#48645,#48646,#48647,#48648,#48649,#48650,
#48651,#48652,#48653,#48654,#48655,#48656,#48657,#48658,#48659,#48660,#48661,
#48662,#48663,#48664,#48665,#48666,#48667,#48668,#48669,#48670,#48671,#48672,
#48673,#48674,#48675,#48676,#48677,#48678,#48679,#48680),.UNSPECIFIED.,
 .F.,.F.,(4,2,2,2,2,2,2,2,2,2,2,2,2,2,2,2,2,2,2,2,2,2,2,2,2,2,2,2,2,2,2,
2,2,2,2,2,2,2,2,2,2,2,2,2,4),(-4.0615787133633,-3.96620177886682,-3.94503108919774,
-3.93181765514419,-3.92951421756921,-3.92829213342944,-3.92728762705765,
-3.92627426614759,-3.92440867070688,-3.91839205846606,-3.80196330535944,
-3.77967963236435,-3.77222240536503,-3.76940715944143,-3.76740557751464,
-3.76659008987622,-3.76606427033867,-3.7654919740136,-3.76480504787816,
-3.763170536333,-3.74960832598282,-3.71984875033243,-3.70071937502966,-3.66351880813675,
-3.61123877065554,-3.60724819991789,-3.60571977798997,-3.60466757844447,
-3.60363737175628,-3.60239662282504,-3.599302266991,-3.57062615652089,-3.52079054086545,
-3.4737166867985,-3.45405731627538,-3.4484113590116,-3.44611753151641,-3.4449354149033,
-3.44394137526668,-3.44332964851857,-3.44276496805675,-3.44204401693983,
-3.4405253381659,-3.43049852344022,-3.40020803169445),.UNSPECIFIED.);
#275=B_SPLINE_CURVE_WITH_KNOTS('',3,(#48682,#48683,#48684,#48685,#48686,
#48687,#48688,#48689,#48690,#48691,#48692,#48693,#48694,#48695,#48696,#48697,
#48698,#48699,#48700,#48701,#48702,#48703,#48704,#48705,#48706,#48707,#48708,
#48709,#48710,#48711,#48712,#48713,#48714,#48715,#48716,#48717,#48718,#48719,
#48720,#48721,#48722,#48723,#48724,#48725,#48726,#48727,#48728,#48729,#48730,
#48731,#48732,#48733,#48734,#48735,#48736,#48737,#48738,#48739,#48740,#48741,
#48742,#48743,#48744,#48745,#48746,#48747,#48748,#48749,#48750,#48751),
 .UNSPECIFIED.,.F.,.F.,(4,3,3,3,3,3,3,3,3,3,3,3,3,3,3,3,3,3,3,3,3,3,3,4),
(466.050844719725,466.143596562294,466.236448811706,466.329354796081,466.422413806425,
466.485382467895,466.578455412171,466.671402251808,466.764250622992,466.857031127648,
466.949776449804,467.042511414905,467.135260833247,467.228109473982,467.321009914593,
467.414065810677,467.485097123367,467.579229131387,467.673226742089,467.767113320224,
467.860900400145,467.95462914991,468.048328493834,468.097305384879),
 .UNSPECIFIED.);
#276=B_SPLINE_CURVE_WITH_KNOTS('',3,(#48752,#48753,#48754,#48755,#48756,
#48757,#48758,#48759,#48760,#48761,#48762,#48763,#48764,#48765,#48766,#48767,
#48768,#48769,#48770,#48771,#48772,#48773,#48774,#48775,#48776,#48777,#48778,
#48779,#48780,#48781,#48782,#48783,#48784,#48785,#48786,#48787,#48788,#48789,
#48790,#48791,#48792,#48793,#48794,#48795,#48796,#48797,#48798,#48799,#48800,
#48801,#48802,#48803,#48804,#48805,#48806,#48807,#48808,#48809,#48810,#48811,
#48812,#48813,#48814,#48815,#48816,#48817,#48818,#48819,#48820,#48821,#48822,
#48823,#48824,#48825,#48826,#48827,#48828,#48829,#48830,#48831,#48832,#48833,
#48834,#48835,#48836,#48837,#48838,#48839,#48840,#48841,#48842,#48843,#48844,
#48845,#48846,#48847,#48848,#48849,#48850,#48851,#48852,#48853,#48854,#48855,
#48856,#48857,#48858,#48859,#48860,#48861,#48862,#48863,#48864,#48865,#48866,
#48867,#48868,#48869,#48870,#48871,#48872,#48873,#48874,#48875,#48876,#48877,
#48878,#48879,#48880,#48881,#48882,#48883,#48884,#48885,#48886,#48887,#48888,
#48889,#48890,#48891,#48892,#48893,#48894,#48895,#48896,#48897,#48898,#48899,
#48900,#48901,#48902,#48903,#48904,#48905,#48906,#48907,#48908,#48909,#48910,
#48911,#48912,#48913,#48914,#48915,#48916,#48917,#48918,#48919,#48920,#48921,
#48922,#48923,#48924,#48925,#48926,#48927,#48928,#48929,#48930,#48931,#48932,
#48933,#48934,#48935,#48936,#48937),.UNSPECIFIED.,.F.,.F.,(4,2,2,2,2,2,
2,2,2,2,2,2,2,2,2,2,2,2,2,2,2,2,2,2,2,2,2,2,2,2,2,2,2,2,2,2,2,2,2,2,2,2,
2,2,2,2,2,2,2,2,2,2,2,2,2,2,2,2,2,2,2,2,2,2,2,2,2,2,2,2,2,2,2,2,2,2,2,2,
2,2,2,2,2,2,2,2,2,2,2,2,2,2,4),(-4.06102333513819,-3.96661297328627,-3.94683356885609,
-3.93828133537681,-3.93694479057649,-3.93625299686735,-3.9356923494225,
-3.9351265088338,-3.9340797865513,-3.93066447296231,-3.87155298263716,-3.82222574212027,
-3.8034392971281,-3.78718506566586,-3.7812897165891,-3.77719386933177,-3.77565164006015,
-3.77471029304505,-3.77369065752855,-3.77235988113401,-3.76955160478619,
-3.74861391313929,-3.74647686426005,-3.70429585091037,-3.67504670677928,
-3.61689596049452,-3.61452905408814,-3.61365635747988,-3.61306620414351,
-3.61249191978958,-3.61179749555171,-3.61012108741465,-3.59522644760756,
-3.5935481312716,-3.59239646518981,-3.51645285402837,-3.4827428536277,-3.46497190228762,
-3.45867175374597,-3.45575880576181,-3.45344224045727,-3.45222227852344,
-3.45122729886878,-3.45022924412357,-3.44844062621916,-3.44302958760913,
-3.37028995110029,-3.32493451580695,-3.29600822902595,-3.29334502975947,
-3.29141458258231,-3.29061058507698,-3.29003430706728,-3.28950817212511,
-3.28879753654037,-3.28741705157541,-3.27706424183957,-3.27534818489528,
-3.18270236713388,-3.15246530018486,-3.13959001225012,-3.13463234365715,
-3.13219291099084,-3.13018735644553,-3.12903744098369,-3.12812711588652,
-3.12710706113729,-3.12520905938198,-3.11892483816865,-3.00433252195369,
-2.98767310454523,-2.97719508497035,-2.96919318877411,-2.96787925868693,
-2.96719214813878,-2.96663166474445,-2.96597699694161,-2.96484410785524,
-2.9605150234889,-2.88625559350889,-2.84263187020004,-2.81580431920211,
-2.81117914581305,-2.80886118231187,-2.80744807022002,-2.80615930686291,
-2.80516399782833,-2.80419706420858,-2.80283854552623,-2.80003546021256,
-2.77063181171653,-2.70090609820099,-2.6921555152646),.UNSPECIFIED.);
#277=B_SPLINE_CURVE_WITH_KNOTS('',3,(#48943,#48944,#48945,#48946,#48947,
#48948,#48949,#48950,#48951,#48952,#48953,#48954,#48955,#48956,#48957,#48958,
#48959,#48960,#48961,#48962,#48963,#48964,#48965,#48966,#48967,#48968,#48969,
#48970,#48971,#48972,#48973,#48974,#48975,#48976,#48977,#48978,#48979,#48980,
#48981,#48982,#48983,#48984,#48985,#48986,#48987,#48988,#48989,#48990,#48991,
#48992,#48993,#48994,#48995,#48996,#48997,#48998,#48999,#49000,#49001,#49002,
#49003,#49004,#49005,#49006,#49007,#49008,#49009,#49010,#49011,#49012,#49013,
#49014,#49015,#49016,#49017,#49018,#49019,#49020,#49021,#49022,#49023,#49024,
#49025,#49026,#49027,#49028,#49029,#49030,#49031,#49032,#49033,#49034,#49035,
#49036,#49037,#49038,#49039,#49040,#49041,#49042,#49043,#49044,#49045,#49046,
#49047,#49048,#49049,#49050,#49051,#49052,#49053,#49054,#49055,#49056,#49057,
#49058,#49059,#49060,#49061,#49062,#49063,#49064,#49065,#49066,#49067,#49068,
#49069,#49070,#49071,#49072,#49073,#49074,#49075,#49076,#49077,#49078,#49079,
#49080,#49081,#49082,#49083,#49084,#49085,#49086,#49087,#49088,#49089,#49090,
#49091,#49092,#49093,#49094,#49095,#49096,#49097,#49098,#49099,#49100,#49101,
#49102,#49103,#49104,#49105,#49106,#49107,#49108,#49109,#49110,#49111,#49112,
#49113,#49114,#49115,#49116,#49117,#49118,#49119,#49120,#49121,#49122,#49123,
#49124,#49125,#49126,#49127,#49128,#49129,#49130,#49131,#49132,#49133,#49134,
#49135,#49136),.UNSPECIFIED.,.F.,.F.,(4,2,2,2,2,2,2,2,2,2,2,2,2,2,2,2,2,
2,2,2,2,2,2,2,2,2,2,2,2,2,2,2,2,2,2,2,2,2,2,2,2,2,2,2,2,2,2,2,2,2,2,2,2,
2,2,2,2,2,2,2,2,2,2,2,2,2,2,2,2,2,2,2,2,2,2,2,2,2,2,2,2,2,2,2,2,2,2,2,2,
2,2,2,2,2,2,2,4),(-1.36992344699479,-1.33960600328324,-1.26228671155231,
-1.23213459145953,-1.23016072994359,-1.2294085412778,-1.22887155089048,
-1.22835978497847,-1.22764679456012,-1.22618974112011,-1.21350048378456,
-1.18806983696264,-1.13244453543704,-1.07382188127391,-1.06998499640528,
-1.06858894017261,-1.06761185348278,-1.06670137986705,-1.06545492751759,
-1.06303707312315,-1.04740332913328,-1.01112232314901,-0.950033619719869,
-0.922931174911829,-0.922605097521007,-0.921691854054946,-0.921230660763885,
-0.920442522312564,-0.908606070033288,-0.90717097083674,-0.906446336991062,
-0.905916622286234,-0.905343299170856,-0.904775673089278,-0.903394366543461,
-0.893473916510318,-0.867904806572996,-0.823313541315134,-0.789348744931029,
-0.786232056619268,-0.750048493467329,-0.746839117141523,-0.745545445941268,
-0.744595685753544,-0.743570734734431,-0.742184772950679,-0.739050318367336,
-0.734865950220565,-0.72461480256142,-0.688649671775339,-0.636737754195658,
-0.587525744593009,-0.584662443851755,-0.583686635801761,-0.583135068269418,
-0.582628240192152,-0.582088947190191,-0.581411745210198,-0.578916009252255,
-0.55346583158862,-0.512237808824646,-0.429930139050887,-0.424603356767535,
-0.422826019385017,-0.421830220116047,-0.420923835426037,-0.419714958969524,
-0.417474413467056,-0.405748283319039,-0.382678751118875,-0.348368915438273,
-0.3191046067704,-0.277362426122141,-0.276979030294106,-0.273870193803622,
-0.262733693484774,-0.261187272214194,-0.26044998771106,-0.25988292888482,
-0.259266772920944,-0.25863313562572,-0.257706302058061,-0.25004211900516,
-0.217471255943138,-0.206023129562492,-0.193655928435844,-0.1623328410385,
-0.105044923905998,-0.101252073628557,-0.0998627891717248,-0.0988875652544676,
-0.097976544012608,-0.0967258052425551,-0.0942873535456371,-0.0912209017053736,
-0.0844695428702945,-0.000961974495844116),.UNSPECIFIED.);
#278=B_SPLINE_CURVE_WITH_KNOTS('',3,(#49137,#49138,#49139,#49140,#49141,
#49142),.UNSPECIFIED.,.F.,.F.,(4,1,1,4),(472.335020342325,473.182047544726,
474.181762200199,474.380490692059),.UNSPECIFIED.);
#279=B_SPLINE_CURVE_WITH_KNOTS('',3,(#49143,#49144,#49145,#49146,#49147,
#49148,#49149,#49150,#49151,#49152,#49153,#49154,#49155,#49156,#49157,#49158,
#49159,#49160,#49161,#49162,#49163,#49164,#49165,#49166,#49167,#49168,#49169,
#49170,#49171,#49172,#49173,#49174,#49175,#49176,#49177,#49178,#49179,#49180,
#49181,#49182,#49183,#49184,#49185,#49186,#49187,#49188,#49189,#49190,#49191,
#49192,#49193,#49194,#49195,#49196,#49197,#49198,#49199,#49200,#49201,#49202,
#49203,#49204,#49205,#49206,#49207,#49208,#49209,#49210,#49211,#49212,#49213,
#49214,#49215,#49216,#49217,#49218,#49219,#49220,#49221,#49222,#49223,#49224,
#49225,#49226,#49227,#49228,#49229,#49230,#49231,#49232,#49233,#49234,#49235,
#49236,#49237,#49238,#49239,#49240,#49241,#49242,#49243,#49244,#49245,#49246,
#49247,#49248,#49249,#49250,#49251,#49252,#49253,#49254,#49255,#49256,#49257,
#49258,#49259,#49260,#49261,#49262,#49263,#49264,#49265,#49266,#49267,#49268,
#49269,#49270,#49271,#49272,#49273,#49274,#49275,#49276,#49277,#49278,#49279,
#49280,#49281,#49282,#49283,#49284,#49285,#49286,#49287,#49288,#49289,#49290,
#49291,#49292,#49293,#49294,#49295,#49296,#49297,#49298,#49299,#49300,#49301,
#49302,#49303,#49304,#49305,#49306,#49307,#49308,#49309,#49310,#49311,#49312,
#49313,#49314,#49315,#49316,#49317,#49318,#49319,#49320,#49321,#49322,#49323,
#49324,#49325,#49326,#49327,#49328,#49329,#49330,#49331,#49332,#49333,#49334,
#49335,#49336,#49337,#49338,#49339,#49340,#49341,#49342,#49343,#49344,#49345,
#49346,#49347,#49348,#49349,#49350,#49351,#49352,#49353,#49354,#49355,#49356,
#49357,#49358,#49359,#49360,#49361,#49362,#49363,#49364,#49365,#49366,#49367,
#49368,#49369,#49370,#49371,#49372,#49373,#49374,#49375,#49376,#49377,#49378,
#49379,#49380,#49381,#49382,#49383,#49384,#49385,#49386,#49387,#49388,#49389,
#49390,#49391,#49392,#49393,#49394,#49395,#49396,#49397,#49398,#49399,#49400,
#49401,#49402,#49403,#49404,#49405,#49406,#49407,#49408,#49409,#49410,#49411,
#49412,#49413,#49414,#49415,#49416,#49417,#49418,#49419,#49420,#49421,#49422,
#49423,#49424,#49425,#49426,#49427,#49428,#49429,#49430,#49431,#49432,#49433,
#49434,#49435,#49436,#49437,#49438,#49439,#49440,#49441,#49442,#49443,#49444,
#49445,#49446,#49447,#49448,#49449,#49450,#49451,#49452,#49453,#49454,#49455,
#49456,#49457,#49458,#49459,#49460,#49461,#49462,#49463,#49464,#49465,#49466),
 .UNSPECIFIED.,.F.,.F.,(4,2,2,2,2,2,2,2,2,2,2,2,2,2,2,2,2,2,2,2,2,2,2,2,
2,2,2,2,2,2,2,2,2,2,2,2,2,2,2,2,2,2,2,2,2,2,2,2,2,2,2,2,2,2,2,2,2,2,2,2,
2,2,2,2,2,2,2,2,2,2,2,2,2,2,2,2,2,2,2,2,2,2,2,2,2,2,2,2,2,2,2,2,2,2,2,2,
2,2,2,2,2,2,2,2,2,2,2,2,2,2,2,2,2,2,2,2,2,2,2,2,2,2,2,2,2,2,2,2,2,2,2,2,
2,2,2,2,2,2,2,2,2,2,2,2,2,2,2,2,2,2,2,2,2,2,2,2,2,2,2,2,2,4),(-2.6921555152646,
-2.64872518836412,-2.64556828097275,-2.64459303618737,-2.64398035314961,
-2.6434118967061,-2.64266641215536,-2.64107969144127,-2.62889557859108,
-2.62680371756745,-2.62565101194808,-2.62384307272071,-2.62365651231036,
-2.62173630501906,-2.61783628235704,-2.56533226983517,-2.52079374687381,
-2.49078619247967,-2.48724121356062,-2.48533250295622,-2.48409141163039,
-2.48292768953092,-2.48198564837255,-2.48096706012537,-2.47907729353888,
-2.47286552646328,-2.36936543701896,-2.32387011012541,-2.32202891283071,
-2.32124010998656,-2.32066646266215,-2.32013669900715,-2.31941236655072,
-2.31797897979877,-2.3062032700755,-2.30454171834748,-2.21542816650337,
-2.17912023648743,-2.16345935447878,-2.16105056887395,-2.15980578344754,
-2.15889528835548,-2.15791699652451,-2.1562280876479,-2.15152772817747,
-2.08015996604046,-2.0305930422031,-2.01993183746673,-2.01786541763354,
-2.01765403785961,-2.01557440502413,-2.01441867610367,-2.01323285592272,
-2.01281808440065,-2.01133220265145,-2.0003366081747,-1.99893119223079,
-1.99821402542402,-1.99768612160929,-1.99711104658864,-1.99631425752895,
-1.99442690601696,-1.9593387143366,-1.85873970573516,-1.85750761155556,
-1.85650250987388,-1.85562547822162,-1.85353222682329,-1.85266089977613,
-1.85087566958439,-1.84889985721392,-1.84064446174111,-1.83801547658754,
-1.8367257094214,-1.83571486839475,-1.83459437209975,-1.83275480607629,
-1.82626791825706,-1.78518121937992,-1.73793799932418,-1.67997671180798,
-1.67638419090264,-1.67531640161721,-1.67474623576602,-1.6741911881303,
-1.6735224257443,-1.6722798977157,-1.67072279480498,-1.61924445570903,-1.53812099080982,
-1.53535101509222,-1.51773605791126,-1.51503005334933,-1.51373899616501,
-1.51272527997245,-1.51161678169669,-1.50983069829253,-1.50437161932364,
-1.47242999474235,-1.4025288931549,-1.36879892504244,-1.36842534310419,
-1.36512993607868,-1.35417583929333,-1.35277211337036,-1.35205543157192,
-1.35152770129138,-1.35095262783457,-1.35017155766544,-1.34836067021856,
-1.34588154857607,-1.25703859919527,-1.1963341120859,-1.1925483604652,-1.19116008665413,
-1.19018507594113,-1.18927385925297,-1.18802223952348,-1.18557993324279,
-1.17023199432998,-1.13482311869531,-1.06576464974758,-1.05453164154305,
-1.05172575296958,-1.04990779043298,-1.04569784063563,-1.04526278381138,
-1.0434941167533,-1.04147447029399,-1.03107390752925,-1.0296914158473,-1.02898021464825,
-1.02845388991006,-1.02787763998223,-1.02709024401996,-1.02525195861575,
-1.02272156276118,-1.01627201777475,-0.991647314633338,-0.943471253523264,
-0.87419101170161,-0.86979847852409,-0.868156561251958,-0.867187678760253,
-0.866274382593825,-0.865007614322277,-0.862491927153914,-0.848277472618057,
-0.829682272329004,-0.795526610535457,-0.749605233450531,-0.721912434360655,
-0.70833121763364,-0.7066958769758,-0.70600872976013,-0.705436304376229,
-0.704843552490359,-0.704244592522621,-0.702570163952914,-0.686510926297019,
-0.673230566397562,-0.661737441512864),.UNSPECIFIED.);
#280=B_SPLINE_CURVE_WITH_KNOTS('',3,(#49471,#49472,#49473,#49474,#49475,
#49476,#49477,#49478,#49479,#49480,#49481,#49482,#49483,#49484,#49485,#49486,
#49487,#49488,#49489,#49490,#49491,#49492,#49493,#49494,#49495,#49496,#49497,
#49498,#49499,#49500,#49501,#49502,#49503,#49504,#49505,#49506,#49507,#49508,
#49509,#49510,#49511,#49512,#49513,#49514,#49515,#49516,#49517,#49518,#49519,
#49520,#49521,#49522,#49523,#49524,#49525,#49526,#49527,#49528,#49529,#49530,
#49531,#49532,#49533,#49534,#49535,#49536,#49537,#49538,#49539,#49540,#49541,
#49542,#49543,#49544,#49545,#49546,#49547,#49548,#49549,#49550,#49551,#49552,
#49553,#49554,#49555,#49556,#49557,#49558,#49559,#49560,#49561,#49562,#49563,
#49564,#49565,#49566,#49567,#49568,#49569,#49570,#49571,#49572,#49573,#49574,
#49575,#49576,#49577,#49578,#49579,#49580,#49581,#49582,#49583,#49584,#49585,
#49586,#49587,#49588,#49589,#49590,#49591,#49592,#49593,#49594,#49595,#49596,
#49597,#49598,#49599,#49600,#49601,#49602,#49603,#49604,#49605,#49606,#49607,
#49608,#49609,#49610,#49611,#49612,#49613,#49614,#49615,#49616,#49617,#49618,
#49619,#49620,#49621,#49622,#49623,#49624,#49625,#49626,#49627,#49628,#49629,
#49630,#49631,#49632,#49633,#49634,#49635,#49636,#49637,#49638,#49639,#49640,
#49641,#49642,#49643,#49644,#49645,#49646,#49647,#49648,#49649,#49650,#49651,
#49652,#49653,#49654,#49655,#49656,#49657,#49658,#49659,#49660,#49661,#49662,
#49663,#49664,#49665,#49666,#49667,#49668,#49669,#49670,#49671,#49672,#49673,
#49674,#49675,#49676,#49677,#49678,#49679,#49680,#49681,#49682,#49683,#49684,
#49685,#49686,#49687,#49688,#49689,#49690,#49691,#49692,#49693,#49694,#49695,
#49696,#49697,#49698,#49699,#49700,#49701,#49702,#49703,#49704,#49705,#49706,
#49707,#49708,#49709,#49710,#49711,#49712,#49713,#49714,#49715,#49716,#49717,
#49718,#49719,#49720,#49721,#49722,#49723,#49724,#49725,#49726,#49727,#49728,
#49729,#49730,#49731,#49732,#49733,#49734,#49735,#49736,#49737,#49738,#49739,
#49740,#49741,#49742,#49743,#49744,#49745,#49746,#49747,#49748,#49749,#49750,
#49751,#49752,#49753,#49754,#49755,#49756,#49757,#49758,#49759,#49760),
 .UNSPECIFIED.,.F.,.F.,(4,2,2,2,2,2,2,2,2,2,2,2,2,2,2,2,2,2,2,2,2,2,2,2,
2,2,2,2,2,2,2,2,2,2,2,2,2,2,2,2,2,2,2,2,2,2,2,2,2,2,2,2,2,2,2,2,2,2,2,2,
2,2,2,2,2,2,2,2,2,2,2,2,2,2,2,2,2,2,2,2,2,2,2,2,2,2,2,2,2,2,2,2,2,2,2,2,
2,2,2,2,2,2,2,2,2,2,2,2,2,2,2,2,2,2,2,2,2,2,2,2,2,2,2,2,2,2,2,2,2,2,2,2,
2,2,2,2,2,2,2,2,2,2,2,2,4),(-3.39933093202269,-3.37192198667737,-3.34555669939565,
-3.33656741287575,-3.33085434678425,-3.32954715876053,-3.32831814166208,
-3.32741003340446,-3.32642544409237,-3.32500147328314,-3.32097765256483,
-3.25608502982255,-3.20763744545644,-3.18876498070904,-3.16966887255641,
-3.16766495064862,-3.16703165411933,-3.1664158000156,-3.16584890998672,
-3.16511169560703,-3.16350714531025,-3.15137772444024,-3.15019968139962,
-3.1495584970972,-3.14912169980331,-3.14833936930078,-3.14688098146186,
-3.1434594199651,-3.11133797412728,-3.04912620331292,-3.0346819883484,-3.00991267076312,
-3.00708486451187,-3.00574159691272,-3.00472391142747,-3.0037630332796,
-3.0024259410061,-2.99895763695626,-2.94491069838879,-2.8839406110529,-2.85784052800934,
-2.84606905885733,-2.84460458268249,-2.84388073922162,-2.84336971631137,
-2.84283170168635,-2.84207527354128,-2.84007473352634,-2.80781205622302,
-2.74465182173471,-2.70340576480221,-2.68729556970097,-2.68434059223959,
-2.68297088216897,-2.68194898125437,-2.68099559361925,-2.67968695080073,
-2.67638859904298,-2.63536793261566,-2.60759610125953,-2.52602947581608,
-2.5224403278124,-2.52142100233404,-2.52079395768511,-2.52023007006467,
-2.51950251754791,-2.51798948763603,-2.50808226364076,-2.44483239826897,
-2.39929628029919,-2.36779597278997,-2.36414698181158,-2.36141352378903,
-2.3600620797709,-2.35904303963629,-2.35808444191119,-2.3567561905675,-2.35334176492262,
-2.30435529145259,-2.27766751052459,-2.22533734471887,-2.20304516325834,
-2.19957465058036,-2.19856508039139,-2.19794489736446,-2.19737925953787,
-2.1966507764747,-2.19545020276176,-2.19091826658226,-2.09747291938542,
-2.06215084063773,-2.04087387003158,-2.03829155567975,-2.03701157738786,
-2.0360966803647,-2.03513337386174,-2.03378726759814,-2.031033219116,-1.98038202712003,
-1.8876861202532,-1.87742622297775,-1.87589726717593,-1.87517437624013,
-1.87460948754367,-1.87398633475508,-1.87296366286417,-1.86936772705566,
-1.78782010630006,-1.74261155588595,-1.73846423448186,-1.73533475790599,
-1.73264165982437,-1.73062221889132,-1.73016494516652,-1.72810240212397,
-1.72628919413808,-1.71870939431408,-1.71588743981392,-1.71452452662425,
-1.71355661623871,-1.71264338533304,-1.71137535790882,-1.70885229179558,
-1.69024767153786,-1.66209718108382,-1.56647665098842,-1.5545092071133,
-1.55291039753953,-1.5521741179042,-1.5516072198842,-1.55099060811522,-1.55001729567529,
-1.54685757238908,-1.49466855338194,-1.42247621071353,-1.41477893170555,
-1.39516709891951,-1.39265453294616,-1.39136917882915,-1.39042161353809,
-1.38939527015229,-1.38800075739516,-1.38481831589471,-1.38055397574252,
-1.36992344699479),.UNSPECIFIED.);
#281=B_SPLINE_CURVE_WITH_KNOTS('',3,(#49762,#49763,#49764,#49765,#49766,
#49767,#49768,#49769,#49770,#49771,#49772,#49773,#49774,#49775,#49776,#49777,
#49778,#49779,#49780,#49781,#49782,#49783,#49784,#49785,#49786,#49787,#49788,
#49789,#49790,#49791,#49792,#49793,#49794,#49795,#49796,#49797,#49798,#49799,
#49800,#49801,#49802,#49803,#49804,#49805,#49806,#49807,#49808,#49809,#49810,
#49811,#49812,#49813,#49814,#49815,#49816,#49817,#49818,#49819,#49820,#49821,
#49822,#49823,#49824,#49825,#49826,#49827,#49828,#49829,#49830,#49831,#49832,
#49833,#49834,#49835,#49836,#49837,#49838,#49839,#49840,#49841,#49842,#49843,
#49844,#49845,#49846,#49847,#49848,#49849,#49850,#49851,#49852,#49853,#49854,
#49855,#49856,#49857,#49858,#49859,#49860,#49861,#49862,#49863,#49864,#49865,
#49866,#49867,#49868,#49869,#49870,#49871),.UNSPECIFIED.,.F.,.F.,(4,2,2,
2,2,2,2,2,2,2,2,2,2,2,2,2,2,2,2,2,2,2,2,2,2,2,2,2,2,2,2,2,2,2,2,2,2,2,2,
2,2,2,2,2,2,2,2,2,2,2,2,2,2,2,4),(-0.661737441512864,-0.633222867219186,
-0.552295341085543,-0.5470940973112,-0.54533405193584,-0.544341694208613,
-0.543434672279343,-0.542219387795267,-0.539949171077573,-0.527667983114906,
-0.443085223762492,-0.423299550443007,-0.406769898725888,-0.402909764926324,
-0.40166206152074,-0.385418117027195,-0.383853040257971,-0.383095921295719,
-0.382557565193185,-0.382046345475579,-0.381498197152693,-0.380792463753194,
-0.377943262255727,-0.373541880672581,-0.359854716308531,-0.337183918662043,
-0.316966016825565,-0.285254450557795,-0.227493595042903,-0.223676619841762,
-0.222283506076079,-0.221307147094467,-0.220396296814355,-0.219147698643439,
-0.216720038907084,-0.201636398544457,-0.172564307606687,-0.143837926692173,
-0.131165460430137,-0.124661871041258,-0.117035008391087,-0.0713093049919375,
-0.0701815573747394,-0.0686406194917836,-0.0662570601790751,-0.0636784513378337,
-0.0611606696905414,-0.0602355252090651,-0.059694050841081,-0.0591841257063379,
-0.0586384187966496,-0.05794023835713,-0.056859184314074,-0.0548314519699521,
-0.000961045134699609),.UNSPECIFIED.);
#282=B_SPLINE_CURVE_WITH_KNOTS('',3,(#49872,#49873,#49874,#49875,#49876,
#49877,#49878,#49879,#49880,#49881,#49882,#49883,#49884,#49885,#49886,#49887,
#49888,#49889,#49890,#49891,#49892,#49893,#49894,#49895,#49896,#49897,#49898,
#49899,#49900,#49901,#49902,#49903,#49904,#49905,#49906,#49907,#49908,#49909,
#49910,#49911,#49912,#49913,#49914,#49915,#49916,#49917,#49918,#49919,#49920,
#49921,#49922,#49923,#49924,#49925,#49926,#49927,#49928,#49929,#49930,#49931,
#49932,#49933,#49934,#49935,#49936,#49937,#49938,#49939,#49940,#49941,#49942,
#49943,#49944,#49945,#49946,#49947,#49948,#49949,#49950,#49951,#49952,#49953,
#49954,#49955,#49956,#49957,#49958,#49959,#49960,#49961,#49962,#49963,#49964,
#49965,#49966,#49967,#49968,#49969,#49970,#49971,#49972,#49973,#49974,#49975,
#49976,#49977,#49978,#49979,#49980,#49981,#49982,#49983,#49984,#49985,#49986,
#49987,#49988,#49989,#49990,#49991,#49992,#49993,#49994,#49995,#49996,#49997,
#49998,#49999,#50000,#50001,#50002,#50003,#50004,#50005,#50006,#50007,#50008,
#50009,#50010,#50011,#50012,#50013,#50014,#50015,#50016,#50017,#50018,#50019,
#50020,#50021,#50022,#50023,#50024,#50025,#50026,#50027,#50028,#50029,#50030,
#50031,#50032,#50033,#50034,#50035,#50036,#50037,#50038,#50039,#50040,#50041,
#50042,#50043,#50044,#50045,#50046,#50047,#50048,#50049,#50050,#50051,#50052,
#50053,#50054,#50055,#50056,#50057,#50058,#50059),.UNSPECIFIED.,.F.,.F.,
(4,2,2,2,2,2,2,2,2,2,2,2,2,2,2,2,2,2,2,2,2,2,2,2,2,2,2,2,2,2,2,2,2,2,2,
2,2,2,2,2,2,2,2,2,2,2,2,2,2,2,2,2,2,2,2,2,2,2,2,2,2,2,2,2,2,2,2,2,2,2,2,
2,2,2,2,2,2,2,2,2,2,2,2,2,2,2,2,2,2,2,2,2,2,4),(-4.06145248375961,-3.97227698131646,
-3.96575458039436,-3.96276577754912,-3.96037755022854,-3.95913741308972,
-3.95813165300121,-3.95712835315958,-3.95531325104445,-3.94969960193822,
-3.85707818763002,-3.83745890205865,-3.81177955682372,-3.79954551730999,
-3.79851433989304,-3.79783715127806,-3.7972979055941,-3.79679113678703,
-3.79623967881305,-3.79526418067788,-3.7924025756618,-3.7431169932631,-3.71159709513579,
-3.67510577031043,-3.65154328374339,-3.63960344985516,-3.63735150872766,
-3.63614022025778,-3.63523365786259,-3.63423929074326,-3.63246891421817,
-3.62719307134317,-3.54546048711246,-3.51954730742542,-3.49120503024035,
-3.48136954807898,-3.47614059758234,-3.47497951316494,-3.47443491034768,
-3.47392558497026,-3.47338274516004,-3.47245047712617,-3.46988524819966,
-3.42835767694418,-3.3867396155417,-3.3406605563784,-3.32504332345435,-3.31932059606169,
-3.31529515802321,-3.31376135947242,-3.31270800327187,-3.31167864965621,
-3.31044132063389,-3.30736801013771,-3.27945993694265,-3.23099597452038,
-3.18840303656109,-3.16988497079114,-3.15424909093175,-3.15252411167739,
-3.15173696962351,-3.15116083330467,-3.15063455741361,-3.14992334393174,
-3.14854060213908,-3.13206683580295,-3.12680923623964,-3.11054758627852,
-3.04052752538214,-2.99952780033866,-2.99304887730472,-2.99121038035081,
-2.99009027879397,-2.9890796273541,-2.9877898726544,-2.98516011497382,-2.96914210582708,
-2.96530442110006,-2.95999782830021,-2.95110637699093,-2.93379038461465,
-2.88251293251839,-2.83208971347903,-2.82980879653136,-2.82894872561336,
-2.82835751757514,-2.82778408380062,-2.82709285196959,-2.82536769233764,
-2.80957264370983,-2.80799096768976,-2.79990499110941,-2.71753453449011,
-2.69253084801131),.UNSPECIFIED.);
#283=B_SPLINE_CURVE_WITH_KNOTS('',3,(#50065,#50066,#50067,#50068,#50069,
#50070,#50071,#50072,#50073,#50074,#50075,#50076,#50077,#50078,#50079,#50080,
#50081,#50082,#50083,#50084,#50085,#50086,#50087,#50088,#50089,#50090,#50091,
#50092,#50093,#50094,#50095,#50096,#50097,#50098,#50099,#50100,#50101,#50102,
#50103,#50104,#50105,#50106,#50107,#50108,#50109,#50110,#50111,#50112,#50113,
#50114,#50115,#50116,#50117,#50118,#50119,#50120,#50121,#50122,#50123,#50124,
#50125,#50126,#50127,#50128,#50129,#50130,#50131,#50132,#50133,#50134,#50135,
#50136,#50137,#50138,#50139,#50140,#50141,#50142,#50143,#50144,#50145,#50146,
#50147,#50148,#50149,#50150,#50151,#50152,#50153,#50154,#50155,#50156,#50157,
#50158,#50159,#50160,#50161,#50162,#50163,#50164,#50165,#50166,#50167,#50168,
#50169,#50170,#50171,#50172,#50173,#50174,#50175,#50176,#50177,#50178,#50179,
#50180,#50181,#50182,#50183,#50184,#50185,#50186,#50187,#50188,#50189,#50190,
#50191,#50192,#50193,#50194,#50195,#50196,#50197,#50198,#50199,#50200,#50201,
#50202,#50203,#50204,#50205,#50206,#50207,#50208,#50209,#50210,#50211,#50212,
#50213,#50214,#50215,#50216,#50217,#50218,#50219,#50220,#50221,#50222,#50223,
#50224,#50225,#50226,#50227,#50228,#50229,#50230,#50231,#50232,#50233,#50234,
#50235,#50236,#50237,#50238,#50239,#50240,#50241,#50242,#50243,#50244,#50245,
#50246,#50247,#50248,#50249,#50250,#50251,#50252,#50253,#50254,#50255,#50256,
#50257,#50258,#50259,#50260,#50261,#50262,#50263,#50264),.UNSPECIFIED.,
 .F.,.F.,(4,2,2,2,2,2,2,2,2,2,2,2,2,2,2,2,2,2,2,2,2,2,2,2,2,2,2,2,2,2,2,
2,2,2,2,2,2,2,2,2,2,2,2,2,2,2,2,2,2,2,2,2,2,2,2,2,2,2,2,2,2,2,2,2,2,2,2,
2,2,2,2,2,2,2,2,2,2,2,2,2,2,2,2,2,2,2,2,2,2,2,2,2,2,2,2,2,2,2,2,4),(-1.36933436101521,
-1.36849737424044,-1.36775242609568,-1.36721734441935,-1.36664751075481,
-1.36588013452935,-1.36419258443954,-1.35105890789208,-1.32617825355882,
-1.25775072372392,-1.2115088765732,-1.20812901691825,-1.20680626804603,
-1.20584892192528,-1.20482868117506,-1.20347132772782,-1.20057710288288,
-1.17520541615952,-1.15368424802282,-1.09318886372733,-1.04867423922206,
-1.0458506686294,-1.04488069969442,-1.04433029017226,-1.04382315898495,
-1.04312869847589,-1.04180666955098,-1.03352227312986,-1.01535355381888,
-0.951112133275545,-0.88913250968735,-0.885332240925437,-0.883941753980511,
-0.882966157361079,-0.882055162289823,-0.880805039758072,-0.878434126459346,
-0.863363712164514,-0.8292129522212,-0.780958762004757,-0.752088677245505,
-0.724534427175619,-0.72259881695029,-0.721852756331595,-0.721317391230185,
-0.720747756095872,-0.719981484735029,-0.718299757207449,-0.698511197228781,
-0.679998440108996,-0.635344910659248,-0.597670822203311,-0.565288731179293,
-0.562163285035677,-0.560884222258155,-0.559938157558921,-0.558910403333568,
-0.557508548738348,-0.555962244033717,-0.545632885144771,-0.516780383488332,
-0.468069109637877,-0.413919649883421,-0.413502609402084,-0.411995167406995,
-0.401027214061324,-0.399623058129805,-0.398906297470013,-0.398378577533726,
-0.397803585514048,-0.397006706012031,-0.396120208476993,-0.3897488305053,
-0.376886358482462,-0.345393146673643,-0.318802188693085,-0.244652875726976,
-0.23984351622686,-0.2381389682103,-0.237157707338317,-0.236248270584041,
-0.235010771603775,-0.233692000152381,-0.231598889120807,-0.21489450850021,
-0.176170901662155,-0.16263152946763,-0.148937304010521,-0.0896189000749925,
-0.0894252369788815,-0.0780966960099142,-0.076522504940367,-0.0757908323711787,
-0.0752245721751104,-0.074605634802611,-0.0739680068213746,-0.0730316125793512,
-0.0713722523270497,-0.0677313842462216,-0.000961580881731712),
 .UNSPECIFIED.);
#284=B_SPLINE_CURVE_WITH_KNOTS('',3,(#50265,#50266,#50267,#50268,#50269,
#50270,#50271,#50272,#50273,#50274,#50275,#50276,#50277,#50278,#50279,#50280,
#50281,#50282,#50283,#50284,#50285,#50286,#50287,#50288,#50289,#50290,#50291,
#50292,#50293,#50294,#50295,#50296,#50297,#50298,#50299,#50300,#50301,#50302,
#50303,#50304,#50305,#50306,#50307,#50308,#50309,#50310,#50311,#50312,#50313,
#50314,#50315,#50316,#50317,#50318,#50319,#50320,#50321,#50322,#50323,#50324,
#50325,#50326,#50327,#50328,#50329,#50330,#50331,#50332,#50333,#50334,#50335,
#50336,#50337,#50338,#50339,#50340,#50341,#50342,#50343,#50344,#50345,#50346,
#50347,#50348,#50349,#50350,#50351,#50352,#50353,#50354,#50355,#50356),
 .UNSPECIFIED.,.F.,.F.,(4,2,2,2,2,2,2,2,2,2,2,2,2,2,2,2,2,2,2,2,2,2,2,2,
2,2,2,2,2,2,2,2,2,2,2,2,2,2,2,2,2,2,2,2,2,4),(-4.06038694981303,-3.99311640574062,
-3.97853380020269,-3.97646565463749,-3.97515763148088,-3.9739280367631,
-3.97301993142903,-3.97203576334703,-3.97031490080506,-3.96538869257994,
-3.88768691103398,-3.87427744171466,-3.86147278894616,-3.82817857312513,
-3.81453214875378,-3.81347329767406,-3.81278458238728,-3.81212973769813,
-3.81162590216822,-3.81105199342522,-3.8099644426968,-3.80619378809069,
-3.74411185386278,-3.72381521715483,-3.70363940834911,-3.66978256971005,
-3.65990787219642,-3.65376312553043,-3.65242697435233,-3.65117705592305,
-3.65026645682214,-3.64929151893622,-3.64761713769636,-3.6430088738072,
-3.56858088678463,-3.52192994391434,-3.49251801522111,-3.49046629297178,
-3.48983092158467,-3.48921363645748,-3.48864722699388,-3.48791309633718,
-3.48632485137972,-3.4746228878599,-3.42502489138987,-3.39933093202269),
 .UNSPECIFIED.);
#285=B_SPLINE_CURVE_WITH_KNOTS('',3,(#50357,#50358,#50359,#50360,#50361,
#50362,#50363,#50364,#50365,#50366,#50367,#50368,#50369,#50370,#50371,#50372,
#50373,#50374,#50375,#50376,#50377,#50378,#50379,#50380,#50381,#50382,#50383,
#50384,#50385,#50386,#50387,#50388,#50389,#50390,#50391,#50392,#50393,#50394,
#50395,#50396,#50397,#50398,#50399,#50400,#50401,#50402,#50403,#50404,#50405,
#50406,#50407,#50408,#50409,#50410,#50411,#50412,#50413,#50414,#50415,#50416,
#50417,#50418,#50419,#50420,#50421,#50422,#50423,#50424,#50425,#50426,#50427,
#50428,#50429,#50430,#50431,#50432,#50433,#50434,#50435,#50436,#50437,#50438,
#50439,#50440,#50441,#50442,#50443,#50444,#50445,#50446,#50447,#50448,#50449,
#50450,#50451,#50452,#50453,#50454,#50455,#50456,#50457,#50458,#50459,#50460,
#50461,#50462,#50463,#50464,#50465,#50466,#50467,#50468,#50469,#50470,#50471,
#50472,#50473,#50474,#50475,#50476,#50477,#50478,#50479,#50480,#50481,#50482,
#50483,#50484,#50485,#50486,#50487,#50488,#50489,#50490,#50491,#50492,#50493,
#50494,#50495,#50496,#50497,#50498,#50499,#50500,#50501,#50502,#50503,#50504,
#50505,#50506,#50507,#50508,#50509,#50510,#50511,#50512,#50513,#50514,#50515,
#50516,#50517,#50518,#50519,#50520,#50521,#50522,#50523,#50524,#50525,#50526,
#50527,#50528,#50529,#50530,#50531,#50532,#50533,#50534,#50535,#50536,#50537,
#50538,#50539,#50540,#50541,#50542,#50543,#50544,#50545,#50546,#50547,#50548,
#50549,#50550,#50551,#50552,#50553,#50554,#50555,#50556,#50557,#50558,#50559,
#50560,#50561,#50562,#50563,#50564,#50565,#50566,#50567,#50568,#50569,#50570,
#50571,#50572,#50573,#50574,#50575,#50576,#50577,#50578,#50579,#50580,#50581,
#50582,#50583,#50584,#50585,#50586,#50587,#50588,#50589,#50590,#50591,#50592,
#50593,#50594,#50595,#50596,#50597,#50598,#50599,#50600,#50601,#50602,#50603,
#50604,#50605,#50606,#50607,#50608,#50609,#50610,#50611,#50612,#50613,#50614,
#50615,#50616,#50617,#50618,#50619,#50620,#50621,#50622,#50623,#50624,#50625,
#50626,#50627,#50628,#50629,#50630,#50631,#50632,#50633,#50634,#50635,#50636,
#50637,#50638),.UNSPECIFIED.,.F.,.F.,(4,2,2,2,2,2,2,2,2,2,2,2,2,2,2,2,2,
2,2,2,2,2,2,2,2,2,2,2,2,2,2,2,2,2,2,2,2,2,2,2,2,2,2,2,2,2,2,2,2,2,2,2,2,
2,2,2,2,2,2,2,2,2,2,2,2,2,2,2,2,2,2,2,2,2,2,2,2,2,2,2,2,2,2,2,2,2,2,2,2,
2,2,2,2,2,2,2,2,2,2,2,2,2,2,2,2,2,2,2,2,2,2,2,2,2,2,2,2,2,2,2,2,2,2,2,2,
2,2,2,2,2,2,2,2,2,2,2,2,2,2,2,4),(-2.69253084801131,-2.67659534086741,-2.67233115381611,
-2.66914873035905,-2.66775423401712,-2.6667279059203,-2.66578035629344,
-2.66449502550178,-2.66198250514788,-2.64237064541017,-2.63611734293786,
-2.62852150405745,-2.55863568053625,-2.51029591885371,-2.50709994609254,
-2.50612261201985,-2.50550508180648,-2.50493847869591,-2.50420413911534,
-2.50261560536728,-2.49091658965511,-2.42591608132343,-2.3817727875377,
-2.36129451684806,-2.34805899146598,-2.34575399205254,-2.34453134974085,
-2.34352652472138,-2.34251296128512,-2.3406473363834,-2.33463333419885,
-2.33319821706952,-2.32967900537661,-2.32824391131659,-2.23138521974221,
-2.18908152713744,-2.18434026469069,-2.1832151305322,-2.18256897880751,
-2.18200785859457,-2.18130985881933,-2.18023489535017,-2.17539990948672,
-2.08099343976646,-2.03138589052011,-2.02433449292952,-2.02237361535553,
-2.02121468562102,-2.02030991772038,-2.01912257097719,-2.01698133034504,
-2.00673403734971,-1.98740923246788,-1.96358538548088,-1.87442151254333,
-1.87290868157109,-1.86194672644113,-1.86054274605871,-1.85982601287126,
-1.85929828292596,-1.85872324884482,-1.85792625575665,-1.85603721608547,
-1.82066310716825,-1.71630543227848,-1.71564846989638,-1.71169838331268,
-1.70798984609041,-1.701130938443,-1.69916754919025,-1.69801950643693,-1.6970228349678,
-1.695782161338,-1.6936019133816,-1.69080170718674,-1.63172767613707,-1.55081761589049,
-1.5491636131825,-1.53874922309969,-1.53736623731261,-1.53665492620697,
-1.53612859101639,-1.53555240277751,-1.53474907888718,-1.53295087629794,
-1.53044950023309,-1.44169627237407,-1.38095680560618,-1.37717223247484,
-1.37578421655003,-1.37480933252135,-1.37389819093343,-1.37264660712492,
-1.37025296011532,-1.35600421121596,-1.32489912865048,-1.25821387302968,
-1.21701056136886,-1.2146020085772,-1.21378445093403,-1.21322938489348,
-1.21272329831184,-1.21203817763839,-1.21075961171867,-1.20347094815355,
-1.18818676320163,-1.16657696981207,-1.10568884124944,-1.08473325258402,
-1.05693412234813,-1.05386371607299,-1.0526268313482,-1.05159755851101,
-1.05054399100491,-1.04948791492806,-1.0466723966505,-1.02329703124528,
-1.00102766028182,-0.947179847137763,-0.901764928424828,-0.90109051379113,
-0.892679008728169,-0.891257475013047,-0.890538311895011,-0.889975253252021,
-0.889343101459854,-0.888686548103145,-0.886435297840818,-0.866468984714367,
-0.846571013924919,-0.796071607600607,-0.7351475487337,-0.73136564627348,
-0.729978010019495,-0.72900320518696,-0.728091988463089,-0.726840069756809,
-0.724444985742037,-0.708916508483105,-0.689335332262786,-0.662385834278714),
 .UNSPECIFIED.);
#286=B_SPLINE_CURVE_WITH_KNOTS('',3,(#50643,#50644,#50645,#50646,#50647,
#50648,#50649,#50650,#50651,#50652,#50653,#50654,#50655,#50656,#50657,#50658,
#50659,#50660,#50661,#50662,#50663,#50664,#50665,#50666,#50667,#50668,#50669,
#50670,#50671,#50672,#50673,#50674,#50675,#50676,#50677,#50678,#50679,#50680,
#50681,#50682,#50683,#50684,#50685,#50686,#50687,#50688,#50689,#50690,#50691,
#50692,#50693,#50694,#50695,#50696,#50697,#50698,#50699,#50700,#50701,#50702,
#50703,#50704,#50705,#50706,#50707,#50708,#50709,#50710,#50711,#50712,#50713,
#50714,#50715,#50716,#50717,#50718,#50719,#50720,#50721,#50722,#50723,#50724,
#50725,#50726,#50727,#50728,#50729,#50730,#50731,#50732,#50733,#50734,#50735,
#50736,#50737,#50738,#50739,#50740,#50741,#50742,#50743,#50744,#50745,#50746,
#50747,#50748,#50749,#50750,#50751,#50752,#50753,#50754,#50755,#50756,#50757,
#50758,#50759,#50760,#50761,#50762,#50763,#50764,#50765,#50766,#50767,#50768,
#50769,#50770,#50771,#50772,#50773,#50774,#50775,#50776,#50777,#50778,#50779,
#50780,#50781,#50782,#50783,#50784,#50785,#50786,#50787,#50788,#50789,#50790,
#50791,#50792,#50793,#50794,#50795,#50796,#50797,#50798,#50799,#50800,#50801,
#50802,#50803,#50804,#50805,#50806,#50807,#50808,#50809,#50810,#50811,#50812,
#50813,#50814,#50815,#50816,#50817,#50818,#50819,#50820,#50821,#50822,#50823,
#50824,#50825,#50826,#50827,#50828,#50829,#50830,#50831,#50832,#50833,#50834,
#50835,#50836,#50837,#50838,#50839,#50840,#50841,#50842,#50843,#50844,#50845,
#50846,#50847,#50848,#50849,#50850,#50851,#50852,#50853,#50854,#50855,#50856,
#50857,#50858,#50859,#50860,#50861,#50862,#50863,#50864,#50865,#50866,#50867,
#50868,#50869,#50870,#50871,#50872,#50873,#50874,#50875,#50876,#50877,#50878,
#50879,#50880,#50881,#50882,#50883,#50884,#50885,#50886,#50887,#50888,#50889,
#50890,#50891,#50892,#50893,#50894,#50895,#50896,#50897,#50898,#50899,#50900,
#50901,#50902,#50903,#50904,#50905,#50906,#50907,#50908,#50909,#50910,#50911,
#50912,#50913,#50914),.UNSPECIFIED.,.F.,.F.,(4,2,2,2,2,2,2,2,2,2,2,2,2,
2,2,2,2,2,2,2,2,2,2,2,2,2,2,2,2,2,2,2,2,2,2,2,2,2,2,2,2,2,2,2,2,2,2,2,2,
2,2,2,2,2,2,2,2,2,2,2,2,2,2,2,2,2,2,2,2,2,2,2,2,2,2,2,2,2,2,2,2,2,2,2,2,
2,2,2,2,2,2,2,2,2,2,2,2,2,2,2,2,2,2,2,2,2,2,2,2,2,2,2,2,2,2,2,2,2,2,2,2,
2,2,2,2,2,2,2,2,2,2,2,2,2,2,4),(-3.39926360491999,-3.37688241372124,-3.33085573661026,
-3.31010026402408,-3.30677728275198,-3.30578369970508,-3.30516714426549,
-3.30460048952005,-3.30386478859867,-3.30226826225606,-3.2903558594644,
-3.22820951070095,-3.18531822881361,-3.16057808733654,-3.15216052732146,
-3.14673164470306,-3.14507118593755,-3.14397477139313,-3.14296430139436,
-3.14167364520367,-3.13903810015613,-3.12289522043311,-3.11735249035576,
-3.03665523616719,-2.98532150665199,-2.98347087261955,-2.98268073535315,
-2.98210713837037,-2.98157816748161,-2.98085601297705,-2.97943022933864,
-2.96785273615781,-2.91813389651933,-2.86174859280646,-2.82946421244397,
-2.82576099653129,-2.82379112754816,-2.822106214782,-2.82103043473098,-2.82001412530571,
-2.81870288412083,-2.81589032349568,-2.80788806142458,-2.80603099107828,
-2.80397428507211,-2.80362661398097,-2.80265129205505,-2.80058279536987,
-2.79896228960569,-2.79775909773326,-2.79644032308168,-2.79026173475653,
-2.78256660812256,-2.72096822484289,-2.66613193654551,-2.66134527932127,
-2.66021689139954,-2.65957015969599,-2.65900931932337,-2.65831267132758,
-2.65724163125085,-2.6524523304737,-2.56586679466431,-2.50461836890784,
-2.50185387630215,-2.49963206463485,-2.49843421343516,-2.49742967552889,
-2.49641649826985,-2.49455186309526,-2.48854325080575,-2.38667680144655,
-2.33921581585797,-2.33748919651981,-2.33672111684828,-2.33615128429757,
-2.33561659838711,-2.33487280320976,-2.33295033390937,-2.30620406550764,
-2.21642171974538,-2.19165711740084,-2.17884348180368,-2.1765591866997,
-2.1753411230007,-2.17433671914366,-2.17332073123874,-2.17144236764913,
-2.16532128625365,-2.05773018496375,-2.03039004660336,-2.02972520199299,
-2.01600240165622,-2.0145066996429,-2.01376681935515,-2.01323313997103,
-2.01266261119445,-2.01189060958376,-2.01014264259688,-1.9697475378102,
-1.92491581213147,-1.88398118915712,-1.87617677930896,-1.8746832707421,
-1.87347293732362,-1.87221695572504,-1.85636444688795,-1.8537430315984,
-1.85245495788034,-1.85144451410148,-1.85032350200536,-1.84848090412271,
-1.84196143920366,-1.80051823707967,-1.70660310011969,-1.69300732646376,
-1.69137148575494,-1.69068424211526,-1.69011178515086,-1.68951905390723,
-1.68863447933368,-1.68624245150182,-1.64728549390265,-1.56130865834456,
-1.53391875099285,-1.53116564128081,-1.52981951327835,-1.52885597214535,
-1.52794067287848,-1.5266598426789,-1.52412640537889,-1.50778165212095,
-1.46816929180748,-1.39754399467805,-1.37042613031333,-1.36933436101521),
 .UNSPECIFIED.);
#287=B_SPLINE_CURVE_WITH_KNOTS('',3,(#50916,#50917,#50918,#50919,#50920,
#50921,#50922,#50923,#50924,#50925,#50926,#50927,#50928,#50929,#50930,#50931,
#50932,#50933,#50934,#50935,#50936,#50937,#50938,#50939,#50940,#50941,#50942,
#50943,#50944,#50945,#50946,#50947,#50948,#50949,#50950,#50951,#50952,#50953,
#50954,#50955,#50956,#50957,#50958,#50959,#50960,#50961,#50962,#50963,#50964,
#50965,#50966,#50967,#50968,#50969,#50970,#50971,#50972,#50973,#50974,#50975,
#50976,#50977,#50978,#50979,#50980,#50981,#50982,#50983,#50984,#50985,#50986,
#50987,#50988,#50989,#50990,#50991,#50992,#50993,#50994,#50995,#50996,#50997,
#50998,#50999,#51000,#51001,#51002,#51003),.UNSPECIFIED.,.F.,.F.,(4,2,2,
2,2,2,2,2,2,2,2,2,2,2,2,2,2,2,2,2,2,2,2,2,2,2,2,2,2,2,2,2,2,2,2,2,2,2,2,
2,2,2,2,4),(-0.662385834278714,-0.6362356243194,-0.572935159665514,-0.569148678402942,
-0.568059012042635,-0.567484485895362,-0.566980387874265,-0.566325587197284,
-0.565637065068376,-0.563004150181575,-0.532566945138726,-0.482984349394012,
-0.413161376047426,-0.408659520818866,-0.407000823382457,-0.406028669866761,
-0.405116581895032,-0.403858231629967,-0.402510593401049,-0.396194179924321,
-0.385961775075733,-0.350101223734935,-0.319129754774269,-0.250344510590648,
-0.246247922402608,-0.245138258140834,-0.24448901178997,-0.243984276130349,
-0.243315621913099,-0.242607710623799,-0.241503487429798,-0.227797881617593,
-0.191841775006461,-0.177979160749078,-0.163556726548981,-0.0902301732190564,
-0.0857084764994424,-0.0840467208243449,-0.0830739458307767,-0.0821620295674787,
-0.0809050969223434,-0.0795594306801829,-0.0774023951194937,-0.000961434712091559),
 .UNSPECIFIED.);
#288=B_SPLINE_CURVE_WITH_KNOTS('',3,(#51004,#51005,#51006,#51007,#51008,
#51009,#51010,#51011,#51012,#51013,#51014,#51015,#51016,#51017,#51018,#51019,
#51020,#51021,#51022,#51023,#51024,#51025,#51026,#51027,#51028,#51029,#51030,
#51031,#51032,#51033,#51034,#51035,#51036,#51037,#51038,#51039,#51040,#51041,
#51042,#51043,#51044,#51045,#51046,#51047,#51048,#51049,#51050,#51051,#51052,
#51053,#51054,#51055,#51056,#51057,#51058,#51059,#51060,#51061,#51062,#51063,
#51064,#51065,#51066,#51067,#51068,#51069,#51070,#51071,#51072,#51073,#51074,
#51075,#51076,#51077,#51078,#51079,#51080,#51081,#51082,#51083,#51084,#51085,
#51086,#51087,#51088,#51089,#51090,#51091,#51092,#51093,#51094,#51095,#51096,
#51097,#51098,#51099,#51100,#51101,#51102,#51103,#51104,#51105,#51106,#51107,
#51108,#51109,#51110,#51111,#51112,#51113,#51114,#51115,#51116,#51117,#51118,
#51119,#51120,#51121,#51122,#51123,#51124,#51125,#51126,#51127,#51128,#51129,
#51130,#51131,#51132,#51133,#51134,#51135,#51136,#51137,#51138,#51139,#51140,
#51141,#51142,#51143,#51144,#51145,#51146,#51147,#51148,#51149,#51150,#51151,
#51152,#51153,#51154,#51155,#51156,#51157,#51158,#51159,#51160,#51161,#51162,
#51163,#51164,#51165,#51166,#51167,#51168,#51169,#51170,#51171,#51172,#51173,
#51174,#51175,#51176,#51177,#51178,#51179,#51180,#51181,#51182,#51183,#51184,
#51185,#51186,#51187,#51188,#51189,#51190,#51191,#51192,#51193,#51194,#51195,
#51196,#51197,#51198,#51199,#51200,#51201,#51202,#51203,#51204,#51205,#51206,
#51207),.UNSPECIFIED.,.F.,.F.,(4,2,2,2,2,2,2,2,2,2,2,2,2,2,2,2,2,2,2,2,
2,2,2,2,2,2,2,2,2,2,2,2,2,2,2,2,2,2,2,2,2,2,2,2,2,2,2,2,2,2,2,2,2,2,2,2,
2,2,2,2,2,2,2,2,2,2,2,2,2,2,2,2,2,2,2,2,2,2,2,2,2,2,2,2,2,2,2,2,2,2,2,2,
2,2,2,2,2,2,2,2,2,4),(-4.06003779901135,-3.99247556607899,-3.98327642325354,
-3.98208888839531,-3.98134609672055,-3.98065245603443,-3.98014552290343,
-3.9795949306341,-3.97862362860304,-3.97579052428501,-3.93036375229143,
-3.90194261785647,-3.8890182780983,-3.87655885592633,-3.84124223908723,
-3.82447698249938,-3.82227339468324,-3.82090826587115,-3.81963730940153,
-3.81872357918545,-3.81775662978758,-3.8161238148827,-3.81178792007458,
-3.74248608791876,-3.71631051501777,-3.68854256132202,-3.66846246694046,
-3.66275864953244,-3.65927967300459,-3.6585299818593,-3.65783137461025,
-3.6572703191131,-3.65662485749805,-3.65553104185684,-3.651585727485,-3.58310780442706,
-3.53581135400636,-3.50541525174032,-3.49928585799241,-3.49795071432104,
-3.4967014360209,-3.49579068843143,-3.49481500812085,-3.49342381552868,
-3.48961800283801,-3.42950415014912,-3.39384110001399,-3.3599735440906,
-3.34473815102985,-3.33957445804294,-3.3363507935214,-3.3356181468158,-3.33493179506936,
-3.33437149984588,-3.33380251675499,-3.33274000228331,-3.32919097722671,
-3.27127493342399,-3.22503303473745,-3.19218976146052,-3.17745427151142,
-3.17509716129976,-3.17385011450039,-3.17293965334823,-3.1719630053122,
-3.17056829007569,-3.16673954333308,-3.10865322532429,-3.03993717606383,
-3.02229796519031,-3.01406910841555,-3.01274937087468,-3.01205546542262,
-3.01154846939859,-3.01099793794804,-3.01002707181006,-3.00719712643014,
-2.96305619733515,-2.90900303525728,-2.87079345129595,-2.85464749899698,
-2.85226144617692,-2.85099423460073,-2.85008100834707,-2.84911256177796,
-2.84774800496388,-2.84491974598542,-2.84232414505121,-2.83584593539642,
-2.83454804119756,-2.83406271689407,-2.83272207328595,-2.83210249487991,
-2.83002100191228,-2.82851452043185,-2.82730933543043,-2.82599193201632,
-2.81984425319159,-2.80373155241326,-2.73262190960314,-2.70560877785445,
-2.69193413772045),.UNSPECIFIED.);
#289=B_SPLINE_CURVE_WITH_KNOTS('',3,(#51213,#51214,#51215,#51216,#51217,
#51218,#51219,#51220,#51221,#51222,#51223,#51224,#51225,#51226,#51227,#51228,
#51229,#51230,#51231,#51232,#51233,#51234,#51235,#51236,#51237,#51238,#51239,
#51240,#51241,#51242,#51243,#51244,#51245,#51246,#51247,#51248,#51249,#51250,
#51251,#51252,#51253,#51254,#51255,#51256,#51257,#51258,#51259,#51260,#51261,
#51262,#51263,#51264,#51265,#51266,#51267,#51268,#51269,#51270,#51271,#51272,
#51273,#51274,#51275,#51276,#51277,#51278,#51279,#51280,#51281,#51282,#51283,
#51284,#51285,#51286,#51287,#51288,#51289,#51290,#51291,#51292,#51293,#51294,
#51295,#51296,#51297,#51298,#51299,#51300,#51301,#51302,#51303,#51304,#51305,
#51306,#51307,#51308,#51309,#51310,#51311,#51312,#51313,#51314,#51315,#51316,
#51317,#51318,#51319,#51320,#51321,#51322,#51323,#51324,#51325,#51326,#51327,
#51328,#51329,#51330,#51331,#51332,#51333,#51334,#51335,#51336,#51337,#51338,
#51339,#51340,#51341,#51342,#51343,#51344,#51345,#51346,#51347,#51348,#51349,
#51350,#51351,#51352,#51353,#51354,#51355,#51356,#51357,#51358,#51359,#51360,
#51361,#51362,#51363,#51364,#51365,#51366,#51367,#51368,#51369,#51370,#51371,
#51372,#51373,#51374,#51375,#51376,#51377,#51378,#51379,#51380,#51381,#51382,
#51383,#51384,#51385,#51386,#51387,#51388,#51389,#51390,#51391,#51392,#51393,
#51394,#51395,#51396,#51397,#51398,#51399,#51400,#51401,#51402,#51403,#51404,
#51405,#51406,#51407,#51408,#51409,#51410,#51411,#51412,#51413,#51414,#51415,
#51416,#51417,#51418,#51419,#51420,#51421,#51422,#51423,#51424,#51425,#51426,
#51427,#51428,#51429,#51430,#51431,#51432,#51433,#51434,#51435,#51436,#51437,
#51438,#51439,#51440,#51441,#51442,#51443,#51444,#51445,#51446),
 .UNSPECIFIED.,.F.,.F.,(4,2,2,2,2,2,2,2,2,2,2,2,2,2,2,2,2,2,2,2,2,2,2,2,
2,2,2,2,2,2,2,2,2,2,2,2,2,2,2,2,2,2,2,2,2,2,2,2,2,2,2,2,2,2,2,2,2,2,2,2,
2,2,2,2,2,2,2,2,2,2,2,2,2,2,2,2,2,2,2,2,2,2,2,2,2,2,2,2,2,2,2,2,2,2,2,2,
2,2,2,2,2,2,2,2,2,2,2,2,2,2,2,2,2,2,2,2,4),(-1.36972866115331,-1.35430997194401,
-1.34824564483208,-1.3463740748379,-1.34535941941148,-1.3443548579261,-1.34315921423531,
-1.34094750382271,-1.33819824590719,-1.30755377187864,-1.24482795670056,
-1.18871876451973,-1.18528938116151,-1.18424106017695,-1.18367494902106,
-1.18311441967272,-1.18242333485335,-1.18108988449808,-1.17261141508242,
-1.15321542119109,-1.10725524971504,-1.08816458999835,-1.02832567851039,
-1.02464529336729,-1.02327378458777,-1.02230350597661,-1.02139105455907,
-1.02015430931416,-1.01775710142411,-1.01472024774376,-1.00805610257389,
-0.988895949462919,-0.936479395883524,-0.889634430730174,-0.863873931128287,
-0.861967648233763,-0.861226542788088,-0.860692564459935,-0.860122288233946,
-0.859351593287961,-0.857610646815456,-0.798810394935583,-0.736376151537241,
-0.726177069204377,-0.721845007348821,-0.720607127498751,-0.719591456642548,
-0.716275734628755,-0.715959719896745,-0.713927816557707,-0.711758767888483,
-0.703007404921325,-0.701072580514405,-0.699817149858467,-0.698810168581269,
-0.697864975882884,-0.696172878102653,-0.690960368653594,-0.68296913169701,
-0.65889523211027,-0.623738112729008,-0.544101845241873,-0.539706736579721,
-0.538567489342269,-0.537911436083862,-0.537356528611114,-0.536673868668313,
-0.535380527024604,-0.527834103198571,-0.512107466612118,-0.487307428114523,
-0.480047917714727,-0.473886023098427,-0.468551835964313,-0.423129430094186,
-0.406241631322227,-0.400629073897618,-0.399308419013051,-0.398103093096133,
-0.396621153826891,-0.394536539994629,-0.393952577968948,-0.392230805156151,
-0.391239845868998,-0.388424203790562,-0.380359797592356,-0.378305904868506,
-0.377013593761457,-0.376002636694435,-0.375059986445843,-0.373962860224534,
-0.370744318807546,-0.366379415448304,-0.355529411918452,-0.340986550386828,
-0.31516807346096,-0.229282002589889,-0.217509081185714,-0.216076102678238,
-0.215351982415232,-0.214822376013614,-0.214248900941553,-0.213460338640914,
-0.211619718701249,-0.166140578246789,-0.107086394450611,-0.101230681528391,
-0.08751281178236,-0.0586609609909284,-0.0556019951975356,-0.0543461603031945,
-0.0534058746940949,-0.0524508639835445,-0.0514444330553131,-0.0501127305584683,
-0.0479889044122154,-0.000960757701424912),.UNSPECIFIED.);
#290=B_SPLINE_CURVE_WITH_KNOTS('',3,(#51447,#51448,#51449,#51450,#51451,
#51452,#51453,#51454,#51455,#51456,#51457,#51458,#51459,#51460,#51461,#51462,
#51463,#51464,#51465,#51466,#51467,#51468,#51469,#51470,#51471,#51472,#51473,
#51474,#51475,#51476,#51477,#51478,#51479,#51480,#51481,#51482,#51483,#51484,
#51485,#51486,#51487,#51488,#51489,#51490,#51491,#51492,#51493,#51494,#51495,
#51496,#51497,#51498,#51499,#51500,#51501,#51502,#51503,#51504,#51505,#51506,
#51507,#51508,#51509,#51510,#51511,#51512,#51513,#51514,#51515,#51516,#51517,
#51518,#51519,#51520,#51521,#51522,#51523,#51524,#51525,#51526,#51527,#51528,
#51529,#51530,#51531,#51532,#51533,#51534,#51535,#51536,#51537,#51538,#51539,
#51540),.UNSPECIFIED.,.F.,.F.,(4,2,2,2,2,2,2,2,2,2,2,2,2,2,2,2,2,2,2,2,
2,2,2,2,2,2,2,2,2,2,2,2,2,2,2,2,2,2,2,2,2,2,2,2,2,2,4),(-4.05994418293563,
-3.97742496221251,-3.95591745462113,-3.9525215555251,-3.95151995039704,
-3.95090154938977,-3.95033538017432,-3.94960328200121,-3.94802608413189,
-3.93661304150904,-3.93453421145722,-3.84551619506739,-3.82564574588448,
-3.79443721997479,-3.79150927338425,-3.79044126209591,-3.78950021289165,
-3.78848076094066,-3.78714953891444,-3.78433783030483,-3.76329528977208,
-3.76075139198099,-3.74413037407835,-3.71360142990771,-3.68952365920941,
-3.63466645529907,-3.62988884968352,-3.62876121806178,-3.62811468361164,
-3.62755387073336,-3.62685707313564,-3.62578546608493,-3.62098822636374,
-3.53372871152031,-3.49647925483208,-3.47947062628942,-3.47337348946682,
-3.46916689058546,-3.46760843225411,-3.46666742301656,-3.46565026235607,
-3.4643330366156,-3.46148858414917,-3.440538193069,-3.4383865921133,-3.43013952628577,
-3.39926360491999),.UNSPECIFIED.);
#291=B_SPLINE_CURVE_WITH_KNOTS('',3,(#51541,#51542,#51543,#51544,#51545,
#51546,#51547,#51548,#51549,#51550,#51551,#51552,#51553,#51554,#51555,#51556,
#51557,#51558,#51559,#51560,#51561,#51562,#51563,#51564,#51565,#51566,#51567,
#51568,#51569,#51570,#51571,#51572,#51573,#51574,#51575,#51576,#51577,#51578,
#51579,#51580,#51581,#51582,#51583,#51584,#51585,#51586,#51587,#51588,#51589,
#51590,#51591,#51592,#51593,#51594,#51595,#51596,#51597,#51598,#51599,#51600,
#51601,#51602,#51603,#51604,#51605,#51606,#51607,#51608,#51609,#51610,#51611,
#51612,#51613,#51614,#51615,#51616,#51617,#51618,#51619,#51620,#51621,#51622,
#51623,#51624,#51625,#51626,#51627,#51628,#51629,#51630,#51631,#51632,#51633,
#51634,#51635,#51636,#51637,#51638,#51639,#51640,#51641,#51642,#51643,#51644,
#51645,#51646,#51647,#51648,#51649,#51650,#51651,#51652,#51653,#51654,#51655,
#51656,#51657,#51658,#51659,#51660,#51661,#51662,#51663,#51664,#51665,#51666,
#51667,#51668,#51669,#51670,#51671,#51672,#51673,#51674,#51675,#51676,#51677,
#51678,#51679,#51680,#51681,#51682,#51683,#51684,#51685,#51686,#51687,#51688,
#51689,#51690,#51691,#51692,#51693,#51694,#51695,#51696,#51697,#51698,#51699,
#51700,#51701,#51702,#51703,#51704,#51705,#51706,#51707,#51708,#51709,#51710,
#51711,#51712,#51713,#51714,#51715,#51716,#51717,#51718,#51719,#51720,#51721,
#51722,#51723,#51724,#51725,#51726,#51727,#51728,#51729,#51730,#51731,#51732,
#51733,#51734,#51735,#51736,#51737,#51738,#51739,#51740,#51741,#51742,#51743,
#51744,#51745,#51746,#51747,#51748,#51749,#51750,#51751,#51752,#51753,#51754,
#51755,#51756,#51757,#51758,#51759,#51760,#51761,#51762,#51763,#51764,#51765,
#51766,#51767,#51768,#51769,#51770,#51771,#51772,#51773,#51774,#51775,#51776,
#51777,#51778,#51779,#51780,#51781,#51782,#51783,#51784,#51785,#51786,#51787,
#51788,#51789,#51790,#51791,#51792,#51793,#51794,#51795,#51796,#51797,#51798,
#51799,#51800,#51801,#51802,#51803,#51804,#51805,#51806,#51807,#51808,#51809,
#51810,#51811,#51812,#51813,#51814,#51815,#51816,#51817,#51818,#51819,#51820,
#51821,#51822,#51823,#51824,#51825,#51826,#51827,#51828,#51829,#51830),
 .UNSPECIFIED.,.F.,.F.,(4,2,2,2,2,2,2,2,2,2,2,2,2,2,2,2,2,2,2,2,2,2,2,2,
2,2,2,2,2,2,2,2,2,2,2,2,2,2,2,2,2,2,2,2,2,2,2,2,2,2,2,2,2,2,2,2,2,2,2,2,
2,2,2,2,2,2,2,2,2,2,2,2,2,2,2,2,2,2,2,2,2,2,2,2,2,2,2,2,2,2,2,2,2,2,2,2,
2,2,2,2,2,2,2,2,2,2,2,2,2,2,2,2,2,2,2,2,2,2,2,2,2,2,2,2,2,2,2,2,2,2,2,2,
2,2,2,2,2,2,2,2,2,2,2,2,4),(-2.69193413772045,-2.69145735838593,-2.68997330443083,
-2.689245374593,-2.68873357346072,-2.68819670361825,-2.68744492800286,-2.68547352272114,
-2.65547796781937,-2.58680177411471,-2.53793584450239,-2.53081688926782,
-2.52892101604539,-2.52777943479029,-2.52677244192067,-2.52551797818855,
-2.52358647665744,-2.51487666090906,-2.41866994866227,-2.39383860033977,
-2.3711108516713,-2.36878748635319,-2.36710217097525,-2.36631506648136,
-2.36574186136412,-2.36521192442235,-2.3644864991012,-2.36267253648183,
-2.34181123097501,-2.32155688579686,-2.2984761144842,-2.25060622600615,
-2.20985362330253,-2.2066949263751,-2.20530455198635,-2.20427880639,-2.20333005938109,
-2.20204044995278,-2.19885468445759,-2.16379390000003,-2.08376281744099,
-2.0587291815934,-2.04545922109416,-2.0439831998168,-2.04326280772771,-2.04275211728246,
-2.0422124695452,-2.0412966561262,-2.03883963564719,-2.03618409062887,-2.03379751553649,
-2.03225553339583,-2.03093709017565,-2.00248582245845,-1.91232972498501,
-1.90601777440918,-1.90141821870513,-1.89935694711617,-1.88577672316944,
-1.88352910702193,-1.88219278083537,-1.88117217700993,-1.88008424839063,
-1.87839029714646,-1.87319923415328,-1.84453990410164,-1.80139608419535,
-1.72629628467729,-1.72568563910069,-1.72178063192054,-1.72069092094317,
-1.72004632358291,-1.719485022662,-1.71878482700419,-1.71740818559085,-1.70776985487326,
-1.68340336932087,-1.56734170257267,-1.56143825524245,-1.55958632079397,
-1.55857556097066,-1.55757056809375,-1.55636811426141,-1.55412671294974,
-1.55133198730227,-1.48499792005256,-1.40829010296201,-1.40733533400589,
-1.40547462430765,-1.39894469299867,-1.39775076067882,-1.39702416468783,
-1.39645868207639,-1.39583729281005,-1.39482278049122,-1.39130678663127,
-1.36853667619183,-1.34371030455154,-1.24750417382756,-1.2388898378797,
-1.23696624828831,-1.23571429689888,-1.2347075842021,-1.23358761238405,
-1.23173395940765,-1.22950363705495,-1.22511433500846,-1.18202525858585,
-1.13012824151556,-1.08563731704082,-1.08426648713809,-1.08268971798973,
-1.08004892132688,-1.07566294774228,-1.07452467646683,-1.07386886761162,
-1.07331397416925,-1.07263109249877,-1.07133661740354,-1.06376473483138,
-1.04801334067934,-1.02517119407404,-0.947801484228192,-0.917594331509372,
-0.914772900805758,-0.913410080182123,-0.91244216292318,-0.911528866612556,
-0.910286191833184,-0.908004867281879,-0.905059220870743,-0.898663123076397,
-0.880525896394444,-0.830366330299761,-0.75689749657802,-0.752708020055922,
-0.751589096091725,-0.750937769931712,-0.750377213351687,-0.749686319658207,
-0.748353925318702,-0.739903514870463,-0.720666292987405,-0.679396098858072,
-0.661817785846039),.UNSPECIFIED.);
#292=B_SPLINE_CURVE_WITH_KNOTS('',3,(#51835,#51836,#51837,#51838,#51839,
#51840,#51841,#51842,#51843,#51844,#51845,#51846,#51847,#51848,#51849,#51850,
#51851,#51852,#51853,#51854,#51855,#51856,#51857,#51858,#51859,#51860,#51861,
#51862,#51863,#51864,#51865,#51866,#51867,#51868,#51869,#51870,#51871,#51872,
#51873,#51874,#51875,#51876,#51877,#51878,#51879,#51880,#51881,#51882,#51883,
#51884,#51885,#51886,#51887,#51888,#51889,#51890,#51891,#51892,#51893,#51894,
#51895,#51896,#51897,#51898,#51899,#51900,#51901,#51902,#51903,#51904,#51905,
#51906,#51907,#51908,#51909,#51910,#51911,#51912,#51913,#51914,#51915,#51916,
#51917,#51918,#51919,#51920,#51921,#51922,#51923,#51924,#51925,#51926,#51927,
#51928,#51929,#51930,#51931,#51932,#51933,#51934,#51935,#51936,#51937,#51938,
#51939,#51940,#51941,#51942,#51943,#51944,#51945,#51946,#51947,#51948,#51949,
#51950,#51951,#51952,#51953,#51954,#51955,#51956,#51957,#51958,#51959,#51960,
#51961,#51962,#51963,#51964,#51965,#51966,#51967,#51968,#51969,#51970,#51971,
#51972,#51973,#51974,#51975,#51976,#51977,#51978,#51979,#51980,#51981,#51982,
#51983,#51984,#51985,#51986,#51987,#51988,#51989,#51990,#51991,#51992,#51993,
#51994,#51995,#51996,#51997,#51998,#51999,#52000,#52001,#52002,#52003,#52004,
#52005,#52006,#52007,#52008,#52009,#52010,#52011,#52012,#52013,#52014,#52015,
#52016,#52017,#52018,#52019,#52020,#52021,#52022,#52023,#52024,#52025,#52026,
#52027,#52028,#52029,#52030,#52031,#52032,#52033,#52034,#52035,#52036,#52037,
#52038,#52039,#52040,#52041,#52042,#52043,#52044,#52045,#52046,#52047,#52048,
#52049,#52050,#52051,#52052,#52053,#52054,#52055,#52056,#52057,#52058,#52059,
#52060,#52061,#52062,#52063,#52064,#52065,#52066,#52067,#52068,#52069,#52070,
#52071,#52072,#52073,#52074,#52075,#52076,#52077,#52078,#52079,#52080,#52081,
#52082,#52083,#52084,#52085,#52086,#52087,#52088,#52089,#52090,#52091,#52092,
#52093,#52094,#52095,#52096,#52097,#52098,#52099,#52100,#52101,#52102,#52103,
#52104,#52105,#52106,#52107,#52108,#52109,#52110,#52111,#52112,#52113,#52114,
#52115,#52116,#52117,#52118,#52119,#52120),.UNSPECIFIED.,.F.,.F.,(4,2,2,
2,2,2,2,2,2,2,2,2,2,2,2,2,2,2,2,2,2,2,2,2,2,2,2,2,2,2,2,2,2,2,2,2,2,2,2,
2,2,2,2,2,2,2,2,2,2,2,2,2,2,2,2,2,2,2,2,2,2,2,2,2,2,2,2,2,2,2,2,2,2,2,2,
2,2,2,2,2,2,2,2,2,2,2,2,2,2,2,2,2,2,2,2,2,2,2,2,2,2,2,2,2,2,2,2,2,2,2,2,
2,2,2,2,2,2,2,2,2,2,2,2,2,2,2,2,2,2,2,2,2,2,2,2,2,2,2,2,2,2,2,4),(-3.39932589205789,
-3.37664605276613,-3.33295005406636,-3.2922924414732,-3.28584711476626,
-3.28401270198473,-3.28289391097012,-3.28188367621363,-3.28059339678401,
-3.27795888724217,-3.26182941768803,-3.25854352732134,-3.2501482751672,
-3.16035385444002,-3.13374173424251,-3.12696445228955,-3.12434056697558,
-3.12303667873142,-3.12224545155251,-3.1215607898935,-3.12100373609016,
-3.12046707377518,-3.11971550236055,-3.11774414646171,-3.08770282907068,
-3.04408149950909,-2.99901702339878,-2.97707835448093,-2.96389188932416,
-2.96158992126389,-2.96036823343809,-2.95936385397638,-2.95835045222884,
-2.95648429361429,-2.95046201323023,-2.83443153499172,-2.80156898383306,
-2.80016498238844,-2.79933231530872,-2.79858354750263,-2.7980246637177,
-2.79749087020683,-2.79675040081671,-2.79525216218959,-2.7814394592779,
-2.78069164271035,-2.69139489710344,-2.66071135190701,-2.64113548415316,
-2.63859862684412,-2.63732783164102,-2.63641424884816,-2.63544748443947,
-2.63408866568762,-2.63128322143616,-2.62367957697548,-2.62186819852085,
-2.61980666134163,-2.61931247891372,-2.61725799075544,-2.6161829955101,
-2.61493598432529,-2.61372534546638,-2.61191326750068,-2.60707292528718,
-2.59795311166414,-2.52116909785941,-2.50047192530725,-2.48018784835006,
-2.47801500043262,-2.4768785810965,-2.4761572361015,-2.47551133018969,-2.47496141507606,
-2.47439949256615,-2.47337181747351,-2.47011069813522,-2.41411707647133,
-2.36371688839609,-2.33721627341591,-2.31824934452656,-2.31573004842992,
-2.3144627939536,-2.31354967459111,-2.31258146936232,-2.31121746253311,
-2.30839102732551,-2.27796120448242,-2.20436367923814,-2.18221998976322,
-2.163095659562,-2.15466518881887,-2.15333368516879,-2.15264301525351,-2.15208251873872,
-2.15143112418033,-2.15031175623636,-2.14611723157317,-2.07656356484937,
-2.03100061670361,-2.01462487206545,-2.01142762061337,-1.99552442799153,
-1.99290069612477,-1.99161226131537,-1.99060189192565,-1.98948133006069,
-1.98764031266588,-1.98113486872217,-1.93983882958115,-1.88882762583447,
-1.85036284286612,-1.84917067840476,-1.8482683523753,-1.83242037978032,
-1.83069392683666,-1.83000254770983,-1.82942913899719,-1.82883811501782,
-1.82796095243577,-1.82556262826323,-1.78705880990871,-1.73588563058796,
-1.67478639615717,-1.67077489374424,-1.66935260643082,-1.66836837506511,
-1.66745997306896,-1.66625436838632,-1.66399768651868,-1.6611798828565,
-1.64090394484499,-1.60353131948829,-1.51343043652783,-1.5086107781585,
-1.50753715947562,-1.50683963513011,-1.5062786283345,-1.50563230640225,
-1.50450613090255,-1.49974999936329,-1.45696013432009,-1.36972866115331),
 .UNSPECIFIED.);
#293=B_SPLINE_CURVE_WITH_KNOTS('',3,(#52122,#52123,#52124,#52125,#52126,
#52127,#52128,#52129,#52130,#52131,#52132,#52133,#52134,#52135,#52136,#52137,
#52138,#52139,#52140,#52141,#52142,#52143,#52144,#52145,#52146,#52147,#52148,
#52149,#52150,#52151,#52152,#52153,#52154,#52155,#52156,#52157,#52158,#52159,
#52160,#52161,#52162,#52163,#52164,#52165,#52166,#52167,#52168,#52169,#52170,
#52171,#52172,#52173,#52174,#52175,#52176,#52177,#52178,#52179,#52180,#52181,
#52182,#52183,#52184,#52185,#52186,#52187,#52188,#52189,#52190,#52191,#52192,
#52193,#52194,#52195,#52196,#52197,#52198,#52199,#52200,#52201,#52202,#52203,
#52204,#52205,#52206,#52207,#52208,#52209,#52210,#52211,#52212,#52213,#52214,
#52215),.UNSPECIFIED.,.F.,.F.,(4,2,2,2,2,2,2,2,2,2,2,2,2,2,2,2,2,2,2,2,
2,2,2,2,2,2,2,2,2,2,2,2,2,2,2,2,2,2,2,2,2,2,2,2,2,2,4),(-0.661817785846039,
-0.631446402549966,-0.594936698900035,-0.591720851839081,-0.590426142407845,
-0.589476182966453,-0.588451554667015,-0.587443401341402,-0.58507720331537,
-0.57005418523331,-0.536081981121245,-0.511038236961451,-0.434371763132626,
-0.433334741118563,-0.429713493102654,-0.428642525482714,-0.428071792347138,
-0.427516904834903,-0.426835569337568,-0.425548596991163,-0.418139527423193,
-0.402628039054871,-0.36025705268546,-0.341038272571705,-0.316338706676212,
-0.297203327417526,-0.290954043984244,-0.271336657129702,-0.268823687320345,
-0.267538157236581,-0.266590477115374,-0.26556402366529,-0.264552679137309,
-0.263207389113299,-0.256922756022098,-0.226064499166746,-0.205907523735348,
-0.111736952927014,-0.107489642422549,-0.105981692504411,-0.105254940934071,
-0.104690929687764,-0.104062964051209,-0.103019489520687,-0.0992174504771558,
-0.0104838575317579,-0.000962328596166258),.UNSPECIFIED.);
#294=B_SPLINE_CURVE_WITH_KNOTS('',3,(#52216,#52217,#52218,#52219,#52220,
#52221,#52222,#52223,#52224,#52225,#52226,#52227,#52228,#52229,#52230,#52231,
#52232,#52233,#52234,#52235,#52236,#52237,#52238,#52239,#52240,#52241,#52242,
#52243,#52244,#52245,#52246,#52247,#52248,#52249,#52250,#52251,#52252,#52253,
#52254,#52255,#52256,#52257,#52258,#52259,#52260,#52261,#52262,#52263,#52264,
#52265,#52266,#52267,#52268,#52269,#52270,#52271,#52272,#52273,#52274,#52275,
#52276,#52277,#52278,#52279,#52280,#52281,#52282,#52283,#52284,#52285,#52286,
#52287,#52288,#52289,#52290,#52291,#52292,#52293,#52294,#52295,#52296,#52297,
#52298,#52299,#52300,#52301,#52302,#52303,#52304,#52305,#52306,#52307,#52308,
#52309,#52310,#52311,#52312,#52313,#52314,#52315,#52316,#52317,#52318,#52319,
#52320,#52321,#52322,#52323,#52324,#52325,#52326,#52327,#52328,#52329,#52330,
#52331,#52332,#52333,#52334,#52335,#52336,#52337,#52338,#52339,#52340,#52341,
#52342,#52343,#52344,#52345,#52346,#52347,#52348,#52349,#52350,#52351,#52352,
#52353,#52354,#52355,#52356,#52357,#52358,#52359,#52360,#52361,#52362,#52363,
#52364,#52365,#52366,#52367,#52368,#52369,#52370,#52371,#52372,#52373,#52374,
#52375,#52376,#52377,#52378,#52379,#52380,#52381,#52382,#52383,#52384,#52385,
#52386,#52387,#52388,#52389,#52390,#52391,#52392,#52393,#52394,#52395,#52396,
#52397,#52398,#52399,#52400,#52401,#52402,#52403,#52404,#52405,#52406,#52407,
#52408,#52409,#52410,#52411,#52412,#52413,#52414,#52415,#52416,#52417,#52418,
#52419,#52420,#52421,#52422,#52423,#52424,#52425,#52426,#52427,#52428,#52429),
 .UNSPECIFIED.,.F.,.F.,(4,2,2,2,2,2,2,2,2,2,2,2,2,2,2,2,2,2,2,2,2,2,2,2,
2,2,2,2,2,2,2,2,2,2,2,2,2,2,2,2,2,2,2,2,2,2,2,2,2,2,2,2,2,2,2,2,2,2,2,2,
2,2,2,2,2,2,2,2,2,2,2,2,2,2,2,2,2,2,2,2,2,2,2,2,2,2,2,2,2,2,2,2,2,2,2,2,
2,2,2,2,2,2,2,2,2,2,4),(-4.06236830518179,-4.01128230784337,-4.00860916091127,
-4.00704905561026,-4.00595357167427,-4.00501093552446,-4.00399938511821,
-4.00270339750265,-4.00013206854681,-3.99184181669663,-3.98994577632168,
-3.98800630375214,-3.98659213524642,-3.98249844406454,-3.98000829183565,
-3.97510366934702,-3.96600766868781,-3.95141074503959,-3.94540833280247,
-3.89508138093323,-3.84637846026233,-3.84452919536455,-3.84373909705527,
-3.84316532270155,-3.84263603764128,-3.84191323327071,-3.84048550189996,
-3.82886490519833,-3.74707957015382,-3.72030872139708,-3.70213371050775,
-3.68607289248382,-3.68365782899963,-3.68264670893793,-3.68162035132604,
-3.6806724144489,-3.67938600890634,-3.67686976370155,-3.65716555553687,
-3.63783979127214,-3.62869838268935,-3.58079267930138,-3.57471057746759,
-3.56747826151506,-3.54205667472033,-3.53055871425514,-3.52261530716523,
-3.52130399711088,-3.52061747540546,-3.52005706631424,-3.51940201963884,
-3.51826735020328,-3.51391931341309,-3.43952122246206,-3.40733610049415,
-3.37717529654029,-3.36303954199801,-3.36070043932541,-3.3596974279773,
-3.35867552560362,-3.3577210476806,-3.35640920602911,-3.35309389099396,
-3.31112875033255,-3.23255705536707,-3.21840971952123,-3.20578194360784,
-3.19948533541297,-3.19825621823781,-3.19758724679695,-3.19708247993021,
-3.19651789758148,-3.19547766980306,-3.19211666374425,-3.13380261064229,
-3.09118375963743,-3.05560503048395,-3.0454221370737,-3.04125824992219,
-3.03815917116431,-3.03678344746364,-3.03575529140895,-3.03480958861689,
-3.03353212264099,-3.03041602661921,-2.99846025627691,-2.90688671050272,
-2.88555454356852,-2.8766574036631,-2.87530720213329,-2.87461243359211,
-2.87410518784067,-2.8735547614057,-2.87258503620628,-2.86976368789951,
-2.82305473929898,-2.76615661413109,-2.74447225970692,-2.72031992525608,
-2.71720227428073,-2.71475117466605,-2.71350358027369,-2.71258924446251,
-2.71162254860925,-2.70999232954388,-2.70567525048565,-2.69332373186839),
 .UNSPECIFIED.);
#295=B_SPLINE_CURVE_WITH_KNOTS('',3,(#52435,#52436,#52437,#52438,#52439,
#52440,#52441,#52442,#52443,#52444,#52445,#52446,#52447,#52448,#52449,#52450,
#52451,#52452,#52453,#52454,#52455,#52456,#52457,#52458,#52459,#52460,#52461,
#52462,#52463,#52464,#52465,#52466,#52467,#52468,#52469,#52470,#52471,#52472,
#52473,#52474,#52475,#52476,#52477,#52478,#52479,#52480,#52481,#52482,#52483,
#52484,#52485,#52486,#52487,#52488,#52489,#52490,#52491,#52492,#52493,#52494,
#52495,#52496,#52497,#52498,#52499,#52500,#52501,#52502,#52503,#52504,#52505,
#52506,#52507,#52508,#52509,#52510,#52511,#52512,#52513,#52514,#52515,#52516,
#52517,#52518,#52519,#52520,#52521,#52522,#52523,#52524,#52525,#52526,#52527,
#52528,#52529,#52530,#52531,#52532,#52533,#52534,#52535,#52536,#52537,#52538,
#52539,#52540,#52541,#52542,#52543,#52544,#52545,#52546,#52547,#52548,#52549,
#52550,#52551,#52552,#52553,#52554,#52555,#52556,#52557,#52558,#52559,#52560,
#52561,#52562,#52563,#52564,#52565,#52566,#52567,#52568,#52569,#52570,#52571,
#52572,#52573,#52574,#52575,#52576),.UNSPECIFIED.,.F.,.F.,(4,3,3,3,3,3,
3,3,3,3,3,3,3,3,3,3,3,3,3,3,3,3,3,3,3,3,3,3,3,3,3,3,3,3,3,3,3,3,3,3,3,3,
3,3,3,3,3,4),(512.079602535136,512.170919108167,512.263992052284,512.356938891763,
512.44978726279,512.542567767289,512.63531308929,512.728048054237,512.820797472426,
512.913646113011,513.006546553474,513.099602449414,513.17063376364,513.263706707811,
513.356653547343,513.449501918419,513.542282422965,513.63502774501,513.727762709999,
513.820512128227,513.913360768848,514.006261209345,514.099317105315,514.170348419112,
514.263421364159,514.35636820457,514.449216576529,514.541997081958,514.634742404887,
514.727477370759,514.820226789868,514.913075431362,515.005975872729,515.099031769554,
515.170063074585,515.263136017659,515.356082856097,515.448931226086,515.541711729555,
515.634457050532,515.727192014461,515.819941431639,515.912790071233,516.005690510712,
516.098746405693,516.169777730058,516.262840343893,516.317081157972),
 .UNSPECIFIED.);
#296=B_SPLINE_CURVE_WITH_KNOTS('',3,(#52577,#52578,#52579,#52580,#52581,
#52582,#52583,#52584,#52585,#52586,#52587,#52588,#52589,#52590,#52591,#52592,
#52593,#52594,#52595,#52596,#52597,#52598,#52599,#52600,#52601,#52602,#52603,
#52604,#52605,#52606,#52607,#52608,#52609,#52610,#52611,#52612,#52613,#52614,
#52615,#52616,#52617,#52618,#52619,#52620,#52621,#52622,#52623,#52624,#52625,
#52626,#52627,#52628,#52629,#52630,#52631,#52632,#52633,#52634,#52635,#52636,
#52637,#52638,#52639,#52640,#52641,#52642,#52643,#52644,#52645,#52646,#52647,
#52648,#52649,#52650,#52651,#52652,#52653,#52654,#52655,#52656,#52657,#52658,
#52659,#52660,#52661,#52662,#52663,#52664,#52665,#52666,#52667,#52668,#52669,
#52670,#52671,#52672,#52673,#52674,#52675,#52676),.UNSPECIFIED.,.F.,.F.,
(4,2,2,2,2,2,2,2,2,2,2,2,2,2,2,2,2,2,2,2,2,2,2,2,2,2,2,2,2,2,2,2,2,2,2,
2,2,2,2,2,2,2,2,2,2,2,2,2,2,4),(-4.06019064732414,-3.96551133596624,-3.93627764245022,
-3.9310228429966,-3.92932187488524,-3.92823296741668,-3.9272139411775,-3.92588326496817,
-3.92307267248462,-3.90203731571564,-3.89950321675288,-3.88289828236199,
-3.80458145762543,-3.78548988001597,-3.77445220310783,-3.77070040604564,
-3.76818790684858,-3.76729489216759,-3.76677007295134,-3.76620400855292,
-3.76547131563236,-3.76389001694167,-3.75235839834927,-3.74884301231658,
-3.74662501750788,-3.71614948388614,-3.69486242393203,-3.64856163202697,
-3.6142754661495,-3.60846921195793,-3.60670336502825,-3.6055999521817,-3.60458583260201,
-3.60328731492125,-3.60053967969616,-3.58194776095191,-3.58042908630198,
-3.57382290133506,-3.49690215555902,-3.46464457663389,-3.45229160446695,
-3.44821598516339,-3.44641292349166,-3.44501142041935,-3.44431005195053,
-3.44376196090874,-3.44321245953694,-3.44224578809134,-3.43944223418908,
-3.39932589205789),.UNSPECIFIED.);
#297=B_SPLINE_CURVE_WITH_KNOTS('',3,(#52677,#52678,#52679,#52680,#52681,
#52682,#52683,#52684,#52685,#52686,#52687,#52688,#52689,#52690,#52691,#52692,
#52693,#52694,#52695,#52696,#52697,#52698,#52699,#52700,#52701,#52702,#52703,
#52704,#52705,#52706,#52707,#52708,#52709,#52710,#52711,#52712,#52713,#52714,
#52715,#52716,#52717,#52718,#52719,#52720,#52721,#52722,#52723,#52724,#52725,
#52726,#52727,#52728,#52729,#52730,#52731,#52732,#52733,#52734,#52735,#52736,
#52737,#52738,#52739,#52740,#52741,#52742,#52743,#52744,#52745,#52746,#52747,
#52748,#52749,#52750,#52751,#52752,#52753,#52754,#52755,#52756,#52757,#52758,
#52759,#52760,#52761,#52762,#52763,#52764,#52765,#52766,#52767,#52768,#52769,
#52770,#52771,#52772,#52773,#52774,#52775,#52776,#52777,#52778,#52779,#52780,
#52781,#52782,#52783,#52784,#52785,#52786,#52787,#52788,#52789,#52790,#52791,
#52792,#52793,#52794,#52795,#52796,#52797,#52798,#52799,#52800,#52801,#52802,
#52803,#52804,#52805,#52806,#52807,#52808,#52809,#52810,#52811,#52812,#52813,
#52814,#52815,#52816,#52817,#52818,#52819,#52820,#52821,#52822,#52823,#52824,
#52825,#52826,#52827,#52828,#52829,#52830,#52831,#52832,#52833,#52834,#52835,
#52836,#52837,#52838,#52839,#52840,#52841,#52842,#52843,#52844,#52845,#52846,
#52847,#52848,#52849,#52850,#52851,#52852,#52853,#52854,#52855,#52856,#52857,
#52858,#52859,#52860,#52861,#52862,#52863,#52864,#52865,#52866,#52867,#52868,
#52869,#52870,#52871,#52872,#52873,#52874,#52875,#52876,#52877,#52878,#52879,
#52880,#52881,#52882,#52883,#52884,#52885,#52886,#52887,#52888,#52889,#52890,
#52891,#52892,#52893,#52894,#52895,#52896,#52897,#52898,#52899,#52900,#52901,
#52902,#52903,#52904,#52905,#52906,#52907,#52908,#52909,#52910,#52911,#52912,
#52913,#52914,#52915,#52916,#52917,#52918,#52919,#52920,#52921,#52922,#52923,
#52924,#52925,#52926,#52927,#52928,#52929,#52930,#52931,#52932,#52933,#52934,
#52935,#52936,#52937,#52938,#52939,#52940,#52941,#52942,#52943,#52944,#52945,
#52946,#52947,#52948),.UNSPECIFIED.,.F.,.F.,(4,2,2,2,2,2,2,2,2,2,2,2,2,
2,2,2,2,2,2,2,2,2,2,2,2,2,2,2,2,2,2,2,2,2,2,2,2,2,2,2,2,2,2,2,2,2,2,2,2,
2,2,2,2,2,2,2,2,2,2,2,2,2,2,2,2,2,2,2,2,2,2,2,2,2,2,2,2,2,2,2,2,2,2,2,2,
2,2,2,2,2,2,2,2,2,2,2,2,2,2,2,2,2,2,2,2,2,2,2,2,2,2,2,2,2,2,2,2,2,2,2,2,
2,2,2,2,2,2,2,2,2,2,2,2,2,2,4),(-2.69332373186839,-2.63590056303955,-2.59806115287555,
-2.57696081092695,-2.55633179412,-2.55302030257022,-2.55202756390987,-2.55141093236035,
-2.55084378590168,-2.55010686759453,-2.54850543205393,-2.53647896298135,
-2.53424559805585,-2.53356139770569,-2.53178653827847,-2.53063530704833,
-2.52405211013857,-2.51354138754007,-2.4731948785474,-2.42847837585149,
-2.39823559538545,-2.39467385090571,-2.39275854985133,-2.39111355398828,
-2.39004547753411,-2.38902535560524,-2.38769319623464,-2.38487928018183,
-2.363812889089,-2.36146198758775,-2.32627655806885,-2.30286396483439,-2.2539710811715,
-2.23339320988599,-2.2300867051748,-2.22909450837485,-2.2284779923434,-2.22791079669378,
-2.22717360116059,-2.22594435968902,-2.21881994646708,-2.12181547515734,
-2.09091683479816,-2.07125626509458,-2.06871605093705,-2.06744420702026,
-2.06653011952601,-2.0655630513402,-2.06420418141462,-2.06139984690182,
-2.0319497580756,-2.0077183012875,-1.91219803341816,-1.90726791750861,-1.90618514411705,
-1.90548461391946,-1.90492316096849,-1.90427851704085,-1.90316067369496,
-1.89851451677803,-1.87424082566735,-1.82662170535717,-1.81308605501974,
-1.75018670688178,-1.746325956503,-1.74492594377872,-1.74394753995088,-1.74303698448542,
-1.74179218349189,-1.73938360035058,-1.72373175461307,-1.68745316548452,
-1.59432399182279,-1.59227809682013,-1.58447714029863,-1.58321097944092,
-1.58246284549766,-1.58189380053572,-1.58129429297067,-1.58035562690714,
-1.57925316911031,-1.57717004566508,-1.55830257712428,-1.54540281725048,
-1.42958403681793,-1.4235771773282,-1.42171203890487,-1.42069835710753,
-1.41969317171171,-1.41846974060338,-1.41616220645593,-1.40288512962007,
-1.38435686890064,-1.34456156946301,-1.27205622854209,-1.261404885607,-1.26001244020086,
-1.25929859360713,-1.25877152233286,-1.25820745791169,-1.2574305703082,
-1.25655874189117,-1.25505942866704,-1.21168957205603,-1.10651447290484,
-1.10039821345671,-1.09851990419571,-1.09750363473058,-1.09649875622884,
-1.09527983596344,-1.09299310275094,-1.08014531899821,-1.05538661335461,
-0.965473652922269,-0.938761057845499,-0.936838413369243,-0.936094375934143,
-0.935559456860022,-0.935021473923919,-0.934287539974073,-0.932728829940132,
-0.93067138694473,-0.925799967028894,-0.910335530259787,-0.866752418091578,
-0.782554567270362,-0.777096263670779,-0.77530104640451,-0.774301476686873,
-0.773304280652919,-0.772060322566885,-0.769655380994483,-0.754093001055015,
-0.718148387247962,-0.679321467808541,-0.662369123431852),.UNSPECIFIED.);
#298=B_SPLINE_CURVE_WITH_KNOTS('',3,(#52954,#52955,#52956,#52957,#52958,
#52959,#52960,#52961,#52962,#52963,#52964,#52965,#52966,#52967,#52968,#52969,
#52970,#52971,#52972,#52973,#52974,#52975,#52976,#52977,#52978,#52979,#52980,
#52981,#52982,#52983,#52984,#52985,#52986,#52987,#52988,#52989,#52990,#52991,
#52992,#52993,#52994,#52995,#52996,#52997,#52998,#52999,#53000,#53001,#53002,
#53003,#53004,#53005,#53006,#53007,#53008,#53009,#53010,#53011,#53012,#53013,
#53014,#53015,#53016,#53017,#53018,#53019,#53020,#53021,#53022,#53023,#53024,
#53025,#53026,#53027,#53028,#53029,#53030,#53031,#53032,#53033,#53034,#53035,
#53036,#53037,#53038,#53039,#53040,#53041,#53042,#53043,#53044,#53045,#53046,
#53047,#53048,#53049,#53050,#53051,#53052,#53053,#53054,#53055,#53056,#53057,
#53058,#53059,#53060,#53061,#53062,#53063,#53064,#53065,#53066,#53067,#53068,
#53069,#53070,#53071,#53072,#53073,#53074,#53075,#53076,#53077,#53078,#53079,
#53080,#53081,#53082,#53083,#53084,#53085,#53086,#53087,#53088,#53089,#53090,
#53091,#53092,#53093,#53094,#53095,#53096,#53097,#53098,#53099,#53100,#53101,
#53102,#53103,#53104,#53105,#53106,#53107,#53108,#53109,#53110,#53111,#53112,
#53113,#53114,#53115,#53116,#53117,#53118,#53119,#53120,#53121,#53122,#53123,
#53124,#53125,#53126,#53127,#53128,#53129,#53130,#53131,#53132,#53133,#53134,
#53135),.UNSPECIFIED.,.F.,.F.,(4,2,2,2,2,2,2,2,2,2,2,2,2,2,2,2,2,2,2,2,
2,2,2,2,2,2,2,2,2,2,2,2,2,2,2,2,2,2,2,2,2,2,2,2,2,2,2,2,2,2,2,2,2,2,2,2,
2,2,2,2,2,2,2,2,2,2,2,2,2,2,2,2,2,2,2,2,2,2,2,2,2,2,2,2,2,2,2,2,2,2,4),
(-1.37013824341392,-1.34237747191845,-1.26296548255655,-1.25536130056935,
-1.24659540766556,-1.24586959228131,-1.23317991477552,-1.23171711750194,
-1.230999393659,-1.23043646945422,-1.22980340814454,-1.22875837730866,-1.22493445215964,
-1.13629518515779,-1.07548947616176,-1.071705691954,-1.0703177875468,-1.0693429263559,
-1.06843176200177,-1.06718007845695,-1.06473717415751,-1.04842685445754,
-1.00958701002103,-0.949541861280324,-0.920595253380862,-0.910248997532136,
-0.908868742418837,-0.908158155007743,-0.907632020484454,-0.907055704647409,
-0.906482907996922,-0.905053682495817,-0.893500756336844,-0.867187556378256,
-0.824917914430684,-0.753413761330077,-0.74899295524278,-0.747346767872416,
-0.746377109018273,-0.74546421707459,-0.744199804330603,-0.741695247766714,
-0.723585523021593,-0.696841802838405,-0.637649801136975,-0.589168997767841,
-0.586328345886029,-0.585355819349327,-0.584804912645701,-0.584297932530326,
-0.583758288439846,-0.583079869336424,-0.58056957833095,-0.555694178605008,
-0.515219253535521,-0.431711702631918,-0.426296719322435,-0.424507560325197,
-0.423509389672865,-0.422512296152171,-0.421266537180775,-0.418851978487372,
-0.403317567111448,-0.367406759777754,-0.342783674404433,-0.318345898600323,
-0.273498021158975,-0.272245526021084,-0.270739915235589,-0.267961432113831,
-0.263697864826172,-0.262571534646786,-0.261918464415451,-0.261357995163237,
-0.260819564611093,-0.260145265755279,-0.259121007977705,-0.246896917217738,
-0.219095594500449,-0.198237662155218,-0.165635642675342,-0.106771597814053,
-0.102935312594607,-0.101539357531473,-0.100562305560897,-0.099651835767735,
-0.0984053446425378,-0.0959872631004007,-0.0929523634159408,-0.0862943093706694,
-0.000962145650915263),.UNSPECIFIED.);
#299=B_SPLINE_CURVE_WITH_KNOTS('',3,(#53136,#53137,#53138,#53139,#53140,
#53141,#53142,#53143,#53144,#53145,#53146,#53147,#53148,#53149,#53150,#53151,
#53152,#53153,#53154,#53155,#53156,#53157,#53158,#53159,#53160,#53161,#53162,
#53163,#53164,#53165,#53166,#53167,#53168,#53169,#53170,#53171,#53172,#53173,
#53174,#53175,#53176,#53177,#53178,#53179,#53180,#53181,#53182,#53183,#53184,
#53185,#53186,#53187,#53188,#53189,#53190,#53191,#53192,#53193,#53194,#53195,
#53196,#53197,#53198,#53199,#53200,#53201,#53202,#53203,#53204,#53205),
 .UNSPECIFIED.,.F.,.F.,(4,3,3,3,3,3,3,3,3,3,3,3,3,3,3,3,3,3,3,3,3,3,3,4),
(516.317081157972,516.409967208446,516.504907855582,516.597664063071,516.690400143587,
516.783140911013,516.879728779642,516.972608388968,517.065554242249,517.158638357035,
517.169492385531,517.262565334695,517.355512179238,517.44836055534,517.54114106491,
517.633886391977,517.72662136198,517.819370785208,517.912219430777,518.005119876201,
518.098175777011,518.169207041004,518.305071793348,518.362787842316),
 .UNSPECIFIED.);
#300=B_SPLINE_CURVE_WITH_KNOTS('',3,(#53207,#53208,#53209,#53210,#53211,
#53212,#53213,#53214,#53215,#53216,#53217,#53218,#53219,#53220,#53221,#53222,
#53223,#53224,#53225,#53226,#53227,#53228,#53229,#53230,#53231,#53232,#53233,
#53234,#53235,#53236,#53237,#53238,#53239,#53240,#53241,#53242,#53243,#53244,
#53245,#53246,#53247,#53248,#53249,#53250,#53251,#53252,#53253,#53254,#53255,
#53256,#53257,#53258,#53259,#53260,#53261,#53262,#53263,#53264,#53265,#53266,
#53267,#53268,#53269,#53270,#53271,#53272,#53273,#53274,#53275,#53276,#53277,
#53278,#53279,#53280,#53281,#53282,#53283,#53284,#53285,#53286,#53287,#53288,
#53289,#53290,#53291,#53292,#53293,#53294,#53295,#53296,#53297,#53298,#53299,
#53300,#53301,#53302,#53303,#53304,#53305,#53306,#53307,#53308,#53309,#53310,
#53311,#53312,#53313,#53314),.UNSPECIFIED.,.F.,.F.,(4,2,2,2,2,2,2,2,2,2,
2,2,2,2,2,2,2,2,2,2,2,2,2,2,2,2,2,2,2,2,2,2,2,2,2,2,2,2,2,2,2,2,2,2,2,2,
2,2,2,2,2,2,2,4),(-0.662369123431852,-0.62745144403119,-0.624894961586772,
-0.615051491018097,-0.613540831864279,-0.612813519464919,-0.612249410799109,
-0.611634339945498,-0.610626291022457,-0.607162547734505,-0.601490992264344,
-0.581649228413477,-0.55393564927306,-0.459707160818077,-0.454073598566679,
-0.452255559620789,-0.45125145906371,-0.450245429418516,-0.449005750843542,
-0.446620867262244,-0.431562342388669,-0.397524861332346,-0.359405694182378,
-0.340783500053336,-0.315020908576646,-0.31191617739949,-0.309633211910726,
-0.309361695135919,-0.308471664010906,-0.307011722181371,-0.305834854723347,
-0.292248539947005,-0.290612998170837,-0.289925803729212,-0.28935335498504,
-0.28882742131339,-0.288245553991981,-0.286732332052735,-0.27124294091145,
-0.249295311213617,-0.158289237902776,-0.152178623612308,-0.150806701167426,
-0.149596139756178,-0.148344922412134,-0.13248898497981,-0.129867251400714,
-0.128579052407423,-0.127568524631218,-0.126447433991131,-0.12460474039766,
-0.118085269625875,-0.0766441399792139,-0.000962579226033729),
 .UNSPECIFIED.);
#301=B_SPLINE_CURVE_WITH_KNOTS('',3,(#53315,#53316,#53317,#53318,#53319,
#53320,#53321,#53322,#53323,#53324,#53325,#53326,#53327,#53328,#53329,#53330,
#53331,#53332,#53333,#53334,#53335,#53336,#53337,#53338,#53339,#53340,#53341,
#53342,#53343,#53344,#53345,#53346,#53347,#53348,#53349,#53350,#53351,#53352,
#53353,#53354,#53355,#53356,#53357,#53358,#53359,#53360,#53361,#53362,#53363,
#53364,#53365,#53366,#53367,#53368,#53369,#53370,#53371,#53372,#53373,#53374,
#53375,#53376,#53377,#53378,#53379,#53380,#53381,#53382,#53383,#53384,#53385,
#53386,#53387,#53388,#53389,#53390,#53391,#53392,#53393,#53394,#53395,#53396,
#53397,#53398,#53399,#53400,#53401,#53402,#53403,#53404,#53405,#53406,#53407,
#53408,#53409,#53410,#53411,#53412,#53413,#53414,#53415,#53416,#53417,#53418,
#53419,#53420,#53421,#53422,#53423,#53424,#53425,#53426,#53427,#53428,#53429,
#53430,#53431,#53432,#53433,#53434,#53435,#53436,#53437,#53438,#53439,#53440,
#53441,#53442,#53443,#53444,#53445,#53446,#53447,#53448,#53449,#53450,#53451,
#53452,#53453,#53454,#53455,#53456,#53457,#53458,#53459,#53460,#53461,#53462,
#53463,#53464,#53465,#53466,#53467,#53468,#53469,#53470,#53471,#53472,#53473,
#53474,#53475,#53476,#53477,#53478,#53479,#53480,#53481,#53482,#53483,#53484,
#53485,#53486,#53487,#53488,#53489,#53490,#53491,#53492,#53493,#53494,#53495,
#53496,#53497,#53498,#53499,#53500,#53501,#53502,#53503,#53504,#53505,#53506,
#53507,#53508,#53509,#53510,#53511,#53512,#53513,#53514,#53515,#53516,#53517,
#53518,#53519,#53520,#53521,#53522,#53523,#53524,#53525,#53526,#53527,#53528,
#53529,#53530,#53531,#53532,#53533,#53534),.UNSPECIFIED.,.F.,.F.,(4,2,2,
2,2,2,2,2,2,2,2,2,2,2,2,2,2,2,2,2,2,2,2,2,2,2,2,2,2,2,2,2,2,2,2,2,2,2,2,
2,2,2,2,2,2,2,2,2,2,2,2,2,2,2,2,2,2,2,2,2,2,2,2,2,2,2,2,2,2,2,2,2,2,2,2,
2,2,2,2,2,2,2,2,2,2,2,2,2,2,2,2,2,2,2,2,2,2,2,2,2,2,2,2,2,2,2,2,2,2,4),
(-4.06149001195427,-4.03430084075442,-4.02977258884284,-4.02861683066207,
-4.02788745406436,-4.02733148857688,-4.02679461843254,-4.026261124383,-4.02552132882982,
-4.0240252627134,-4.01027274796171,-4.00596483989454,-3.99467961431301,
-3.99071061390817,-3.90714195909425,-3.88237788159706,-3.86958043597391,
-3.86729753140544,-3.86608002678159,-3.86517331928053,-3.86403968739449,
-3.86213891302951,-3.85582587781367,-3.74921804381687,-3.72811942667567,
-3.71330537273624,-3.70621129912855,-3.70494359438975,-3.70438826729269,
-3.70385075405932,-3.70331633483153,-3.70257319468605,-3.70065396998791,
-3.67408357459449,-3.63177721987689,-3.62675265488348,-3.6209528511424,
-3.61415174664876,-3.60598534833864,-3.59577693627203,-3.56189537819281,
-3.5468795548363,-3.54449741845942,-3.54325874171467,-3.54225331094599,
-3.54124962932948,-3.53943185231182,-3.53379544543375,-3.44006046768866,
-3.40660510040486,-3.39091792117336,-3.38596044878126,-3.38387664956146,
-3.38230212462293,-3.38156531356056,-3.38102852077311,-3.38049520577073,
-3.37975639214039,-3.37826460419857,-3.36466423763384,-3.36267115939298,
-3.36095443124507,-3.35920947213016,-3.35611519840963,-3.2742723284145,
-3.26070926712454,-3.23619314107547,-3.22375222098135,-3.22148674059388,
-3.2202727793912,-3.21936621866287,-3.21837384312357,-3.21661236562687,
-3.21139771615466,-3.1303180441815,-3.08397060084227,-3.06821989416106,
-3.06314202052297,-3.06102098153343,-3.05990430519525,-3.0589553434277,
-3.05835411470745,-3.0577864242783,-3.05704427519897,-3.05579742965874,
-3.04834617983115,-3.04581822934454,-2.9451099789324,-2.90218874050175,
-2.89900821338615,-2.89761435505547,-2.89658842155797,-2.8956411833345,
-2.89435619424656,-2.89184410346205,-2.87222633116237,-2.86696597218873,
-2.85995248443672,-2.77377371676683,-2.73873789556053,-2.73731231196971,
-2.73647081687014,-2.73573073418203,-2.73516918636213,-2.73463967760853,
-2.73391536676175,-2.73248103515623,-2.72065634548908,-2.7182387527232,
-2.69318633084655),.UNSPECIFIED.);
#302=B_SPLINE_CURVE_WITH_KNOTS('',3,(#53539,#53540,#53541,#53542,#53543,
#53544,#53545,#53546,#53547,#53548,#53549,#53550,#53551,#53552,#53553,#53554,
#53555,#53556,#53557,#53558,#53559,#53560,#53561,#53562,#53563,#53564,#53565,
#53566,#53567,#53568,#53569,#53570,#53571,#53572,#53573,#53574,#53575,#53576,
#53577,#53578,#53579,#53580,#53581,#53582,#53583,#53584,#53585,#53586,#53587,
#53588,#53589,#53590,#53591,#53592,#53593,#53594,#53595,#53596,#53597,#53598,
#53599,#53600,#53601,#53602,#53603,#53604,#53605,#53606,#53607,#53608,#53609,
#53610,#53611,#53612,#53613,#53614,#53615,#53616,#53617,#53618,#53619,#53620,
#53621,#53622,#53623,#53624,#53625,#53626,#53627,#53628,#53629,#53630,#53631,
#53632,#53633,#53634,#53635,#53636,#53637,#53638,#53639,#53640,#53641,#53642,
#53643,#53644,#53645,#53646,#53647,#53648,#53649,#53650,#53651,#53652,#53653,
#53654,#53655,#53656,#53657,#53658,#53659,#53660,#53661,#53662,#53663,#53664,
#53665,#53666,#53667,#53668,#53669,#53670,#53671,#53672,#53673,#53674,#53675,
#53676,#53677,#53678,#53679,#53680,#53681,#53682,#53683,#53684,#53685,#53686,
#53687,#53688,#53689,#53690,#53691,#53692,#53693,#53694,#53695,#53696,#53697,
#53698,#53699,#53700,#53701,#53702,#53703,#53704,#53705,#53706,#53707,#53708,
#53709,#53710,#53711,#53712,#53713,#53714,#53715,#53716,#53717,#53718,#53719,
#53720,#53721,#53722,#53723,#53724,#53725,#53726,#53727,#53728,#53729,#53730,
#53731,#53732,#53733,#53734,#53735,#53736,#53737,#53738,#53739,#53740,#53741,
#53742,#53743,#53744,#53745,#53746,#53747,#53748,#53749,#53750,#53751,#53752,
#53753,#53754,#53755,#53756,#53757,#53758,#53759,#53760,#53761,#53762,#53763,
#53764,#53765,#53766,#53767,#53768,#53769,#53770,#53771,#53772,#53773,#53774,
#53775,#53776,#53777,#53778,#53779,#53780,#53781,#53782,#53783,#53784,#53785,
#53786,#53787,#53788,#53789,#53790,#53791,#53792,#53793,#53794,#53795,#53796,
#53797,#53798,#53799,#53800,#53801,#53802,#53803,#53804,#53805,#53806,#53807,
#53808,#53809,#53810,#53811,#53812,#53813,#53814,#53815,#53816,#53817,#53818,
#53819,#53820,#53821,#53822,#53823,#53824,#53825,#53826,#53827,#53828,#53829,
#53830,#53831,#53832,#53833,#53834),.UNSPECIFIED.,.F.,.F.,(4,2,2,2,2,2,
2,2,2,2,2,2,2,2,2,2,2,2,2,2,2,2,2,2,2,2,2,2,2,2,2,2,2,2,2,2,2,2,2,2,2,2,
2,2,2,2,2,2,2,2,2,2,2,2,2,2,2,2,2,2,2,2,2,2,2,2,2,2,2,2,2,2,2,2,2,2,2,2,
2,2,2,2,2,2,2,2,2,2,2,2,2,2,2,2,2,2,2,2,2,2,2,2,2,2,2,2,2,2,2,2,2,2,2,2,
2,2,2,2,2,2,2,2,2,2,2,2,2,2,2,2,2,2,2,2,2,2,2,2,2,2,2,2,2,2,2,2,2,4),(-3.39990807077895,
-3.38040660328844,-3.34866766661436,-3.33914485573359,-3.33316968616272,
-3.33184440072165,-3.33060222175386,-3.32969230693305,-3.32871336946001,
-3.32731052388335,-3.32342893520583,-3.26359940006235,-3.22172400779769,
-3.1716315570116,-3.16977654414896,-3.16897668541224,-3.16840125339318,
-3.16787438866942,-3.16716057016105,-3.16576744110638,-3.15508367140835,
-3.11251470375477,-3.05238795228073,-3.03637952601627,-3.01212308458557,
-3.00923325288756,-3.00787791706218,-3.00685822535848,-3.0059006862434,
-3.00457655017696,-3.0011871397329,-2.95416996011485,-2.8979467095119,-2.84863583019543,
-2.84683654492155,-2.84604889145538,-2.84547568407799,-2.84494596089086,
-2.84422127502957,-2.84278595387785,-2.83094280495201,-2.83016267713157,
-2.8297733276619,-2.82706156377725,-2.82536928172015,-2.82362717237232,
-2.81880760933122,-2.80805950114032,-2.74525323139849,-2.70512836055002,
-2.68932956373854,-2.68636256433413,-2.68499024746307,-2.6839675989178,
-2.68301437624201,-2.68170730361202,-2.67841990809102,-2.63808502327443,
-2.55934942475775,-2.54642007452257,-2.53283966987829,-2.52497447856393,
-2.52364952353526,-2.5229544202497,-2.52239350017703,-2.52182944595065,
-2.52079169904626,-2.51745058121227,-2.5133094474349,-2.51216770457176,
-2.51042068833676,-2.50761096435117,-2.50491026473328,-2.50081370012467,
-2.49086450692796,-2.4035980887951,-2.36996552231238,-2.36616982633216,
-2.36329490059547,-2.36194440115669,-2.36092534309872,-2.35996619185918,
-2.35863632018816,-2.35521309223996,-2.30554112729674,-2.2786093836318,
-2.22511129654473,-2.20943281412998,-2.20192717358904,-2.20063573008572,
-2.19995347531968,-2.19939858885528,-2.19882852159025,-2.19776072359094,
-2.19416654971323,-2.13515068532766,-2.08586228671401,-2.04325549219508,
-2.04036258537386,-2.03902150996979,-2.0380039144187,-2.03704195638369,
-2.03543484447454,-2.03126032968916,-2.01045218997788,-1.98781184729252,
-1.93712022100112,-1.88177086144202,-1.87854146259793,-1.87751750538504,
-1.87695627175528,-1.87639506981587,-1.8756950394239,-1.87431887846997,
-1.86468977114958,-1.84035880938954,-1.74981029116488,-1.7205967840737,
-1.71779876424528,-1.71644165901951,-1.71547525974014,-1.71456132708982,
-1.71328893729937,-1.71074485705234,-1.6918941968336,-1.66302596664332,
-1.56477314682159,-1.55617688403716,-1.55474568459255,-1.55403214436791,
-1.55346835826835,-1.5528397679191,-1.55181425263314,-1.54816927035647,
-1.49540073323149,-1.42244268210306,-1.41643427660268,-1.41490473331247,
-1.41367568772917,-1.41267045482983,-1.3967854237545,-1.39416199335293,
-1.3928734568801,-1.39186289285044,-1.39074199697456,-1.38890016081082,
-1.3825248885946,-1.37013824341392),.UNSPECIFIED.);
#303=B_SPLINE_CURVE_WITH_KNOTS('',3,(#53835,#53836,#53837,#53838,#53839,
#53840,#53841,#53842,#53843,#53844,#53845,#53846,#53847,#53848,#53849,#53850,
#53851,#53852,#53853,#53854,#53855,#53856,#53857,#53858,#53859,#53860,#53861,
#53862,#53863,#53864,#53865,#53866,#53867,#53868,#53869,#53870,#53871,#53872,
#53873,#53874,#53875,#53876,#53877,#53878,#53879,#53880,#53881,#53882,#53883,
#53884,#53885,#53886,#53887,#53888,#53889,#53890,#53891,#53892,#53893,#53894,
#53895,#53896,#53897,#53898,#53899,#53900,#53901,#53902,#53903,#53904,#53905,
#53906,#53907,#53908,#53909,#53910,#53911,#53912,#53913,#53914,#53915,#53916,
#53917,#53918,#53919,#53920,#53921,#53922,#53923,#53924,#53925,#53926,#53927,
#53928,#53929,#53930,#53931,#53932,#53933,#53934,#53935,#53936,#53937,#53938,
#53939,#53940,#53941,#53942,#53943,#53944,#53945,#53946,#53947,#53948,#53949,
#53950,#53951,#53952,#53953,#53954,#53955,#53956,#53957,#53958,#53959,#53960,
#53961,#53962,#53963,#53964,#53965,#53966,#53967,#53968,#53969,#53970,#53971,
#53972,#53973,#53974,#53975,#53976,#53977,#53978,#53979,#53980,#53981,#53982,
#53983,#53984,#53985,#53986,#53987,#53988,#53989,#53990,#53991,#53992,#53993,
#53994,#53995,#53996,#53997,#53998,#53999,#54000,#54001,#54002,#54003,#54004,
#54005,#54006,#54007,#54008,#54009,#54010,#54011,#54012,#54013,#54014,#54015,
#54016,#54017,#54018,#54019,#54020,#54021,#54022,#54023,#54024,#54025,#54026,
#54027,#54028,#54029,#54030,#54031,#54032,#54033,#54034,#54035,#54036,#54037,
#54038,#54039,#54040,#54041,#54042,#54043,#54044,#54045,#54046,#54047,#54048,
#54049,#54050,#54051,#54052,#54053,#54054,#54055,#54056,#54057,#54058,#54059,
#54060,#54061,#54062,#54063,#54064,#54065,#54066,#54067,#54068,#54069,#54070,
#54071,#54072,#54073,#54074,#54075,#54076,#54077,#54078,#54079,#54080,#54081,
#54082,#54083,#54084,#54085,#54086,#54087,#54088,#54089,#54090,#54091,#54092,
#54093,#54094,#54095,#54096,#54097,#54098,#54099,#54100,#54101,#54102,#54103,
#54104,#54105,#54106,#54107,#54108,#54109,#54110,#54111,#54112,#54113,#54114,
#54115,#54116,#54117,#54118,#54119,#54120,#54121,#54122),.UNSPECIFIED.,
 .F.,.F.,(4,2,2,2,2,2,2,2,2,2,2,2,2,2,2,2,2,2,2,2,2,2,2,2,2,2,2,2,2,2,2,
2,2,2,2,2,2,2,2,2,2,2,2,2,2,2,2,2,2,2,2,2,2,2,2,2,2,2,2,2,2,2,2,2,2,2,2,
2,2,2,2,2,2,2,2,2,2,2,2,2,2,2,2,2,2,2,2,2,2,2,2,2,2,2,2,2,2,2,2,2,2,2,2,
2,2,2,2,2,2,2,2,2,2,2,2,2,2,2,2,2,2,2,2,2,2,2,2,2,2,2,2,2,2,2,2,2,2,2,2,
2,2,2,2,4),(-2.69318633084655,-2.68468189971131,-2.62901886980189,-2.59358385261486,
-2.57815888471765,-2.57576037604458,-2.57451821440602,-2.57351246849581,
-2.57251055381831,-2.5707017714161,-2.56513527608284,-2.47342691501159,
-2.41619156214142,-2.41460209223925,-2.41333750240447,-2.41269922255045,
-2.41214846386,-2.41159184424319,-2.41059046552659,-2.407533750704,-2.3580483760135,
-2.32737650073408,-2.2926250573767,-2.26783909042529,-2.25505787256037,
-2.25277505005589,-2.25155724634622,-2.25055278214558,-2.24953649855788,
-2.24765690425763,-2.24152630608467,-2.1334703514287,-2.1061900057124,-2.09196065723888,
-2.0904647881606,-2.08974051398886,-2.08922928407664,-2.08869114322145,
-2.08793467795128,-2.08593475518338,-2.08451547365857,-2.03241931032881,
-1.95849902994206,-1.95229565717286,-1.95090908787588,-1.94970350773231,
-1.94820413214907,-1.94612142112026,-1.94550970731586,-1.9440935927618,
-1.94353075188207,-1.94193049841695,-1.93819732358864,-1.931382205116,-1.92942365180125,
-1.92827670120633,-1.92727993124663,-1.92603778776043,-1.92364041427127,
-1.90825815619092,-1.87298490227813,-1.77853232995525,-1.7767398253688,
-1.77573850044467,-1.77430844652868,-1.77243137117405,-1.76829925197024,
-1.76718595702541,-1.76653585629744,-1.76603117125563,-1.76536346649817,
-1.76414018999852,-1.75794442464571,-1.74559339366462,-1.72211834279851,
-1.61415189567692,-1.60802408774217,-1.60614466948463,-1.60512833425635,
-1.60414383647961,-1.60295883475556,-1.60168921461032,-1.59971259122766,
-1.59599216804081,-1.56345809253146,-1.47561408669336,-1.46704572282714,
-1.46399299293052,-1.46280719644719,-1.46201637039835,-1.45915605143732,
-1.45826620015512,-1.4565340040094,-1.44582585880636,-1.44443152638571,
-1.4437172976525,-1.44319023010916,-1.44261469843859,-1.441814879094,-1.4399092042381,
-1.43728906151824,-1.40923195361318,-1.29023571293427,-1.28464740773419,
-1.28283561186476,-1.28183298996764,-1.28084765808855,-1.27964078075811,
-1.27834061043929,-1.27629139472202,-1.27238181543328,-1.23704138054412,
-1.13764055517906,-1.13448748439908,-1.12261122048989,-1.12101582918796,
-1.12028017225954,-1.11971334997043,-1.11909641257351,-1.11810176608883,
-1.114771190778,-1.09394592935953,-1.03630271046631,-0.965617323296009,
-0.961241320247126,-0.959602150303799,-0.958633919089758,-0.957640265737019,
-0.956356591841733,-0.954950286968531,-0.952648400346053,-0.948066379927323,
-0.936484854562949,-0.892272423768784,-0.803605205890611,-0.798912359964746,
-0.797849018916853,-0.797154649172445,-0.796649853878687,-0.796020666371372,
-0.794971525543444,-0.791109871842227,-0.702525002647637,-0.662616381948172),
 .UNSPECIFIED.);
#304=B_SPLINE_CURVE_WITH_KNOTS('',3,(#54128,#54129,#54130,#54131,#54132,
#54133,#54134,#54135,#54136,#54137,#54138,#54139,#54140,#54141,#54142,#54143,
#54144,#54145,#54146,#54147,#54148,#54149,#54150,#54151,#54152,#54153,#54154,
#54155,#54156,#54157,#54158,#54159,#54160,#54161,#54162,#54163,#54164,#54165,
#54166,#54167,#54168,#54169,#54170,#54171,#54172,#54173,#54174,#54175,#54176,
#54177,#54178,#54179,#54180,#54181,#54182,#54183,#54184,#54185,#54186,#54187,
#54188,#54189,#54190,#54191,#54192,#54193,#54194,#54195,#54196,#54197,#54198,
#54199,#54200,#54201,#54202,#54203,#54204,#54205,#54206,#54207,#54208,#54209,
#54210,#54211,#54212,#54213,#54214,#54215,#54216,#54217,#54218,#54219,#54220,
#54221,#54222,#54223,#54224,#54225,#54226,#54227,#54228,#54229,#54230,#54231,
#54232,#54233,#54234,#54235,#54236,#54237,#54238,#54239,#54240,#54241,#54242,
#54243,#54244,#54245,#54246,#54247,#54248,#54249,#54250,#54251,#54252,#54253,
#54254,#54255,#54256,#54257,#54258,#54259,#54260,#54261,#54262,#54263,#54264,
#54265,#54266,#54267,#54268,#54269),.UNSPECIFIED.,.F.,.F.,(4,3,3,3,3,3,
3,3,3,3,3,3,3,3,3,3,3,3,3,3,3,3,3,3,3,3,3,3,3,3,3,3,3,3,3,3,3,3,3,3,3,3,
3,3,3,3,3,4),(530.929158456835,531.052637619016,531.16549756215,531.258593500593,
531.351563238514,531.444434384569,531.537237389033,531.630005035794,531.72276212552,
531.815533443563,531.908403502849,532.001325128654,532.09440160901,532.165212217623,
532.25831400871,532.351290023229,532.44416785562,532.536978127893,532.629753395939,
532.722518449069,532.815298061554,532.908176871882,533.001107515518,533.094193352236,
533.164926873096,533.257859329747,533.350665369314,533.443372805973,533.536012735091,
533.628617739324,533.72121280114,533.813822888242,533.906533935418,533.999297525186,
534.092219217153,534.164641528569,534.257899915445,534.351031676825,534.444064216637,
534.537027017635,534.629953427148,534.722868062142,534.81579552324,534.908818599269,
535.001891738338,535.095115714291,535.164356184042,535.166163310789),
 .UNSPECIFIED.);
#305=B_SPLINE_CURVE_WITH_KNOTS('',3,(#54270,#54271,#54272,#54273,#54274,
#54275,#54276,#54277,#54278,#54279,#54280,#54281,#54282,#54283,#54284,#54285,
#54286,#54287,#54288,#54289,#54290,#54291,#54292,#54293,#54294,#54295,#54296,
#54297,#54298,#54299,#54300,#54301,#54302,#54303,#54304,#54305,#54306,#54307,
#54308,#54309,#54310,#54311,#54312,#54313,#54314,#54315,#54316,#54317,#54318,
#54319,#54320,#54321,#54322,#54323,#54324,#54325,#54326,#54327,#54328,#54329,
#54330,#54331,#54332,#54333,#54334,#54335,#54336,#54337,#54338,#54339,#54340,
#54341,#54342,#54343,#54344,#54345,#54346,#54347,#54348,#54349,#54350,#54351,
#54352,#54353,#54354,#54355,#54356,#54357,#54358,#54359),.UNSPECIFIED.,
 .F.,.F.,(4,2,2,2,2,2,2,2,2,2,2,2,2,2,2,2,2,2,2,2,2,2,2,2,2,2,2,2,2,2,2,
2,2,2,2,2,2,2,2,2,2,2,2,2,4),(-4.06120165931072,-3.99556616212286,-3.98100786531949,
-3.97893812531483,-3.9776297672892,-3.97640015224412,-3.97549263921484,
-3.97450970358573,-3.97279253435601,-3.96788668347697,-3.89165199918798,
-3.87798823616661,-3.86490937232147,-3.83116870365376,-3.81724161128324,
-3.81603487504353,-3.81528433947467,-3.81458531640765,-3.81402452781977,
-3.81337990397929,-3.81228989916152,-3.80838144823366,-3.74246203805211,
-3.70730130462808,-3.67235221308252,-3.66228138304682,-3.65604127753915,
-3.65469821697044,-3.65344307205196,-3.65253117973898,-3.65155723056532,
-3.64989048068315,-3.64533780914025,-3.5723954348527,-3.52500010899046,
-3.49620307353646,-3.4930899070106,-3.49236473420255,-3.49168361836464,
-3.49112850877089,-3.49055724885437,-3.48948388855584,-3.48584250936362,
-3.42682380920632,-3.39990807077895),.UNSPECIFIED.);
#306=B_SPLINE_CURVE_WITH_KNOTS('',3,(#54361,#54362,#54363,#54364,#54365,
#54366,#54367,#54368,#54369,#54370,#54371,#54372,#54373,#54374,#54375,#54376,
#54377,#54378,#54379,#54380,#54381,#54382,#54383,#54384,#54385,#54386,#54387,
#54388,#54389,#54390,#54391,#54392,#54393,#54394,#54395,#54396,#54397,#54398,
#54399,#54400,#54401,#54402,#54403,#54404,#54405,#54406,#54407,#54408,#54409,
#54410,#54411,#54412,#54413,#54414,#54415,#54416,#54417,#54418,#54419,#54420,
#54421,#54422,#54423,#54424,#54425,#54426,#54427,#54428,#54429,#54430,#54431,
#54432,#54433,#54434,#54435,#54436,#54437,#54438,#54439,#54440,#54441,#54442,
#54443,#54444,#54445,#54446,#54447,#54448,#54449,#54450,#54451,#54452,#54453,
#54454,#54455,#54456,#54457,#54458),.UNSPECIFIED.,.F.,.F.,(4,2,2,2,2,2,
2,2,2,2,2,2,2,2,2,2,2,2,2,2,2,2,2,2,2,2,2,2,2,2,2,2,2,2,2,2,2,2,2,2,2,2,
2,2,2,2,2,2,4),(-0.662616381948172,-0.64164880803953,-0.637897976118936,
-0.636515187629546,-0.635541726181257,-0.634549081404025,-0.633278685576807,
-0.63189086355378,-0.629633248732558,-0.625170855294313,-0.61399416417033,
-0.572785370659433,-0.493947957375361,-0.493711805681332,-0.492791178666353,
-0.490673153084149,-0.488474518141173,-0.476513162116398,-0.474914391141096,
-0.474178044652392,-0.473611046546962,-0.47299424284865,-0.472000616741548,
-0.468680689247441,-0.447967400117738,-0.394237912593299,-0.366862630515129,
-0.318228718518348,-0.314817303857046,-0.313489208844909,-0.312530376067834,
-0.311531151009546,-0.310217224666995,-0.308769271225943,-0.306367744686909,
-0.30151465508055,-0.289003716759519,-0.260179951078527,-0.157145848280909,
-0.156458975464507,-0.152608438781245,-0.151524390496064,-0.150881020782156,
-0.150324841857773,-0.14962528217131,-0.148251833042149,-0.138708384617437,
-0.109414066723253,-0.00125715268977482),.UNSPECIFIED.);
#307=B_SPLINE_CURVE_WITH_KNOTS('',3,(#54459,#54460,#54461,#54462,#54463,
#54464,#54465,#54466,#54467,#54468,#54469,#54470,#54471,#54472,#54473,#54474,
#54475,#54476,#54477,#54478,#54479,#54480,#54481,#54482,#54483,#54484,#54485,
#54486,#54487,#54488,#54489,#54490,#54491,#54492,#54493,#54494,#54495,#54496,
#54497,#54498,#54499,#54500,#54501,#54502,#54503,#54504,#54505,#54506,#54507,
#54508,#54509,#54510,#54511,#54512,#54513,#54514,#54515,#54516,#54517,#54518,
#54519,#54520,#54521,#54522,#54523,#54524,#54525,#54526,#54527,#54528,#54529,
#54530,#54531,#54532,#54533,#54534,#54535,#54536,#54537,#54538,#54539,#54540,
#54541,#54542,#54543,#54544,#54545,#54546,#54547,#54548,#54549,#54550,#54551,
#54552,#54553,#54554,#54555,#54556,#54557,#54558,#54559,#54560,#54561,#54562,
#54563,#54564,#54565,#54566,#54567,#54568,#54569,#54570,#54571,#54572,#54573,
#54574,#54575,#54576,#54577,#54578,#54579,#54580,#54581,#54582,#54583,#54584,
#54585,#54586,#54587,#54588,#54589,#54590,#54591,#54592,#54593,#54594,#54595,
#54596,#54597,#54598,#54599,#54600,#54601,#54602,#54603,#54604,#54605,#54606,
#54607,#54608,#54609,#54610,#54611,#54612,#54613,#54614,#54615,#54616,#54617,
#54618,#54619,#54620,#54621,#54622,#54623,#54624,#54625,#54626,#54627,#54628,
#54629,#54630,#54631,#54632,#54633,#54634,#54635,#54636,#54637,#54638,#54639,
#54640,#54641,#54642,#54643,#54644,#54645,#54646,#54647,#54648,#54649,#54650,
#54651,#54652,#54653,#54654,#54655,#54656,#54657,#54658,#54659,#54660,#54661,
#54662,#54663,#54664,#54665,#54666,#54667,#54668,#54669,#54670,#54671,#54672,
#54673,#54674),.UNSPECIFIED.,.F.,.F.,(4,2,2,2,2,2,2,2,2,2,2,2,2,2,2,2,2,
2,2,2,2,2,2,2,2,2,2,2,2,2,2,2,2,2,2,2,2,2,2,2,2,2,2,2,2,2,2,2,2,2,2,2,2,
2,2,2,2,2,2,2,2,2,2,2,2,2,2,2,2,2,2,2,2,2,2,2,2,2,2,2,2,2,2,2,2,2,2,2,2,
2,2,2,2,2,2,2,2,2,2,2,2,2,2,2,2,2,2,4),(1.37016181069821,1.42817268469703,
1.43200789933298,1.4334043543174,1.43438203013633,1.43537430296662,1.43663677632357,
1.43801348135637,1.44024370600046,1.44463111947928,1.48764134481077,1.54213760195462,
1.57822754550834,1.59336649479065,1.59490244891858,1.59565235976803,1.59618873660573,
1.59670049655204,1.5974293882397,1.59895029045889,1.61458255189288,1.63988811921059,
1.66725202696257,1.69662547519539,1.75179430896636,1.75529151678636,1.75663302485728,
1.75759481634359,1.75859105417611,1.75988892862895,1.76131698188804,1.76367177007154,
1.76839864651118,1.78047706797543,1.80758781690462,1.85791906130342,1.91404750363126,
1.9174869532328,1.91853600457507,1.91910199293259,1.91966253425858,1.92035349183607,
1.92168516994251,1.93010503266359,1.94914762418543,2.02148620295153,2.07495196764682,
2.07841802830152,2.07975558937835,2.08071725606204,2.08171578725386,2.08302255946685,
2.08446068187745,2.08683800228604,2.09162384915754,2.10389959102975,2.13178495443518,
2.1826741908711,2.21568600659663,2.21886486444212,2.22407936510792,2.2262480248409,
2.22708150158334,2.22874362089204,2.23955254204174,2.24095159668956,2.24166736716192,
2.24219514445802,2.24277072113446,2.24356978772966,2.24547012952699,2.24808092581734,
2.27595191071345,2.30190133861818,2.31035013218035,2.33953350588949,2.39758232981042,
2.40117975856853,2.40253829688532,2.40350531502331,2.40450077042442,2.40578913804006,
2.40720226860933,2.4095201336109,2.41414480801579,2.42586936524387,2.45139749110119,
2.50069788894983,2.55973013283072,2.56333889153213,2.5644085081129,2.56497901478315,
2.56553397610908,2.5662158261787,2.56750507697796,2.57496088242439,2.59056097061397,
2.60402290728547,2.71272255386578,2.71880183510393,2.72385000642219,2.72558885160803,
2.72657683649139,2.72756438226155,2.72853609321891,2.72976473459772,2.73164427745407,
2.73916942421928),.UNSPECIFIED.);
#308=B_SPLINE_CURVE_WITH_KNOTS('',3,(#54678,#54679,#54680,#54681,#54682,
#54683,#54684,#54685,#54686,#54687,#54688,#54689,#54690,#54691,#54692,#54693,
#54694,#54695,#54696,#54697,#54698,#54699,#54700,#54701,#54702,#54703,#54704,
#54705,#54706,#54707,#54708,#54709,#54710,#54711,#54712,#54713,#54714,#54715,
#54716,#54717,#54718,#54719,#54720,#54721,#54722,#54723,#54724,#54725,#54726,
#54727,#54728,#54729,#54730,#54731,#54732,#54733,#54734,#54735,#54736,#54737,
#54738,#54739,#54740,#54741,#54742,#54743,#54744,#54745,#54746,#54747,#54748,
#54749,#54750),.UNSPECIFIED.,.F.,.F.,(4,3,3,3,3,3,3,3,3,3,3,3,3,3,3,3,3,
3,3,3,3,3,3,3,4),(-4.09274904019423,-3.99885862189133,-3.91013003463561,
-3.82151667028217,-3.73299492467159,-3.64126355488995,-3.55284687784964,
-3.46444494479893,-3.37603656732219,-3.28760055766733,-3.19906748037989,
-3.11047662341899,-3.02175922454557,-2.9991439664185,-2.9113117185417,-2.82359170340724,
-2.73595935458353,-2.64838791647642,-2.56084790305327,-2.47331725290167,
-2.38577391662778,-2.29814419020479,-2.21046845995505,-2.12265849831354,
-2.0615024666646),.UNSPECIFIED.);
#309=B_SPLINE_CURVE_WITH_KNOTS('',3,(#54754,#54755,#54756,#54757,#54758),
 .UNSPECIFIED.,.F.,.F.,(4,1,4),(0.,0.999714655472842,1.11004521091312),
 .UNSPECIFIED.);
#310=B_SPLINE_CURVE_WITH_KNOTS('',3,(#54760,#54761,#54762,#54763,#54764,
#54765,#54766,#54767,#54768,#54769,#54770,#54771,#54772,#54773,#54774,#54775,
#54776,#54777,#54778,#54779,#54780,#54781,#54782,#54783,#54784,#54785,#54786,
#54787,#54788,#54789,#54790,#54791,#54792,#54793,#54794,#54795,#54796,#54797,
#54798,#54799,#54800,#54801,#54802,#54803,#54804,#54805,#54806,#54807,#54808,
#54809,#54810,#54811,#54812,#54813,#54814,#54815,#54816,#54817,#54818,#54819,
#54820,#54821,#54822,#54823,#54824,#54825,#54826,#54827,#54828,#54829,#54830,
#54831,#54832,#54833,#54834,#54835,#54836,#54837,#54838,#54839,#54840,#54841,
#54842,#54843,#54844,#54845,#54846,#54847,#54848,#54849,#54850,#54851,#54852,
#54853,#54854,#54855,#54856,#54857,#54858,#54859,#54860,#54861,#54862,#54863,
#54864,#54865,#54866,#54867,#54868,#54869,#54870,#54871,#54872,#54873,#54874,
#54875,#54876,#54877,#54878,#54879,#54880,#54881,#54882,#54883,#54884,#54885,
#54886,#54887,#54888,#54889,#54890,#54891,#54892,#54893,#54894,#54895,#54896,
#54897,#54898,#54899,#54900,#54901,#54902,#54903,#54904,#54905,#54906,#54907,
#54908,#54909,#54910,#54911,#54912,#54913,#54914,#54915,#54916,#54917,#54918,
#54919,#54920,#54921,#54922,#54923,#54924,#54925,#54926,#54927,#54928,#54929,
#54930,#54931,#54932,#54933,#54934,#54935,#54936,#54937,#54938,#54939,#54940,
#54941,#54942,#54943,#54944,#54945,#54946,#54947,#54948,#54949,#54950,#54951,
#54952,#54953,#54954,#54955,#54956,#54957,#54958,#54959,#54960,#54961,#54962,
#54963,#54964,#54965,#54966,#54967,#54968,#54969,#54970,#54971,#54972,#54973,
#54974,#54975,#54976,#54977,#54978,#54979,#54980,#54981,#54982,#54983,#54984,
#54985),.UNSPECIFIED.,.F.,.F.,(4,3,3,3,3,3,3,3,3,3,3,3,3,3,3,3,3,3,3,3,
3,3,3,3,3,3,3,3,3,3,3,3,3,3,3,3,3,3,3,3,3,3,3,3,3,3,3,3,3,3,3,3,3,3,3,3,
3,3,3,3,3,3,3,3,3,3,3,3,3,3,3,3,3,3,3,4),(1.11004521091312,1.19650607737286,
1.28285954163267,1.37243076279679,1.45864998573532,1.54484568426876,1.63104074825189,
1.71725806627711,1.80356937260469,1.88993662696758,1.9764320828088,1.99942931094568,
2.08812745070002,2.17671106230774,2.26520376443174,2.35694628968009,2.44533579641836,
2.53371128164707,2.62209394913821,2.71050500255831,2.79901433144695,2.88758211323926,
2.97627757213889,2.99914396641851,3.08785485581244,3.17645390358261,3.26496469990875,
3.35670144015657,3.44511561604432,3.53351817191689,3.62193029548219,3.71037317610221,
3.79891771398502,3.88752272128331,3.97625809233711,3.99885862189134,4.08728386431003,
4.17559277707174,4.26380932330746,4.35565481756455,4.44376630278272,4.53186355987564,
4.61996809333743,4.70810140790274,4.79633499959244,4.88462787176457,4.97305177594552,
4.99857327736417,5.08715380295404,5.17561969285427,5.26399471606801,5.35578136816414,
5.4440540997554,5.53231335681461,5.6205804771028,5.70887679887865,5.79727320596014,
5.88572898664489,5.97431467292538,5.99828793283701,6.08685951668191,6.17531672428596,
6.26368333420257,6.35547324096598,6.44373829164684,6.53199015295223,6.62025017209036,
6.70853969699712,6.79692979659758,6.88537954726025,6.97395966042451,6.99800258830984,
7.09680951298944,7.19522907349122,7.29422968025973,7.39323028702825),
 .UNSPECIFIED.);
#311=B_SPLINE_CURVE_WITH_KNOTS('',3,(#54987,#54988,#54989,#54990,#54991,
#54992,#54993,#54994,#54995,#54996),.UNSPECIFIED.,.F.,.F.,(4,1,1,1,1,1,
1,4),(7.3932305180927,7.99771724378266,8.99743189925548,9.9971465547283,
10.9968612102011,11.9965758656739,12.9962905211468,13.6764158252723),
 .UNSPECIFIED.);
#312=B_SPLINE_CURVE_WITH_KNOTS('',3,(#54998,#54999,#55000,#55001,#55002,
#55003,#55004,#55005,#55006,#55007),.UNSPECIFIED.,.F.,.F.,(4,1,1,1,1,1,
1,4),(13.6764158252723,13.9960051766196,14.9957198320924,15.9954344875653,
16.9951491430381,17.994863798511,18.9945784539838,19.9595964226787),
 .UNSPECIFIED.);
#313=B_SPLINE_CURVE_WITH_KNOTS('',3,(#55009,#55010,#55011,#55012,#55013,
#55014,#55015,#55016,#55017,#55018,#55019,#55020,#55021,#55022,#55023,#55024,
#55025,#55026,#55027,#55028,#55029,#55030,#55031,#55032,#55033,#55034,#55035,
#55036,#55037,#55038,#55039,#55040,#55041,#55042,#55043,#55044,#55045,#55046,
#55047,#55048,#55049,#55050,#55051,#55052,#55053,#55054,#55055,#55056,#55057,
#55058,#55059,#55060,#55061,#55062,#55063,#55064,#55065,#55066,#55067,#55068,
#55069,#55070,#55071,#55072,#55073,#55074,#55075,#55076,#55077,#55078,#55079,
#55080,#55081,#55082,#55083,#55084,#55085,#55086,#55087,#55088,#55089,#55090,
#55091,#55092,#55093,#55094,#55095,#55096,#55097,#55098,#55099,#55100,#55101,
#55102,#55103,#55104,#55105,#55106,#55107,#55108,#55109,#55110,#55111,#55112,
#55113,#55114,#55115,#55116,#55117,#55118,#55119,#55120,#55121,#55122,#55123,
#55124,#55125,#55126,#55127,#55128,#55129,#55130,#55131,#55132,#55133,#55134,
#55135,#55136,#55137,#55138,#55139,#55140,#55141,#55142,#55143,#55144,#55145,
#55146,#55147,#55148,#55149,#55150,#55151,#55152,#55153,#55154,#55155,#55156,
#55157,#55158,#55159,#55160,#55161,#55162,#55163,#55164,#55165,#55166,#55167,
#55168,#55169,#55170,#55171,#55172,#55173,#55174,#55175,#55176,#55177,#55178,
#55179,#55180,#55181,#55182,#55183,#55184,#55185,#55186,#55187,#55188,#55189,
#55190,#55191,#55192,#55193,#55194,#55195,#55196,#55197,#55198,#55199,#55200,
#55201,#55202,#55203,#55204,#55205,#55206,#55207,#55208,#55209,#55210,#55211,
#55212,#55213,#55214,#55215,#55216,#55217,#55218,#55219,#55220,#55221,#55222,
#55223,#55224,#55225,#55226,#55227,#55228,#55229,#55230,#55231,#55232,#55233,
#55234,#55235,#55236,#55237),.UNSPECIFIED.,.F.,.F.,(4,3,3,3,3,3,3,3,3,3,
3,3,3,3,3,3,3,3,3,3,3,3,3,3,3,3,3,3,3,3,3,3,3,3,3,3,3,3,3,3,3,3,3,3,3,3,
3,3,3,3,3,3,3,3,3,3,3,3,3,3,3,3,3,3,3,3,3,3,3,3,3,3,3,3,3,3,4),(19.9596011324519,
19.9942931094567,20.0828452660075,20.1712826660522,20.2596291138166,20.3514264452057,
20.4396705717611,20.5279012623694,20.6161398857834,20.7044078113348,20.7927761166749,
20.8812039325379,20.9697620733111,20.9940077649295,21.0825599166399,21.1709973117995,
21.2593437546402,21.3511410878605,21.4393852094268,21.5276158950304,21.6158545134292,
21.7041224339604,21.792490734298,21.8809185451629,21.9694766809828,21.9937224204023,
22.0822745714392,22.1707119659024,22.2590584080244,22.3508557415058,22.4390998623023,
22.5273305471184,22.615569164713,22.7038370844238,22.7922053839211,22.8806331939328,
22.9691913288876,22.9934370758752,23.0819892286553,23.1704266248874,23.2587730688019,
23.3505704016202,23.4388145242568,23.5270452109275,23.6152838303892,23.7035517519777,
23.7919200533592,23.8803478652613,23.9689060021007,23.993151731348,24.0817038833189,
24.1701412787335,24.2584877218233,24.350285054948,24.438529176747,24.5267598625767,
24.614998481195,24.7032664019385,24.7916347024769,24.8800625135359,24.9686206495389,
24.9928663868208,25.0814185387661,25.1698559341527,25.258202377212,25.3499997103472,
25.4382438321097,25.5264745179007,25.6147131364782,25.7029810571788,25.7913493576714,
25.879777168683,25.9683353046363,25.9925810422937,26.108658292392,26.2221398067425,
26.2427863295604),.UNSPECIFIED.);
#314=B_SPLINE_CURVE_WITH_KNOTS('',3,(#55239,#55240,#55241,#55242,#55243,
#55244,#55245,#55246,#55247,#55248),.UNSPECIFIED.,.F.,.F.,(4,1,1,1,1,1,
1,4),(26.2427864396315,26.9922956977665,27.9920103532393,28.9917250087122,
29.991439664185,30.9911543196578,31.9908689751307,32.525971746811),
 .UNSPECIFIED.);
#315=B_SPLINE_CURVE_WITH_KNOTS('',3,(#55250,#55251,#55252,#55253,#55254,
#55255,#55256,#55257,#55258,#55259,#55260,#55261,#55262,#55263,#55264,#55265,
#55266,#55267,#55268,#55269,#55270,#55271,#55272,#55273,#55274,#55275,#55276,
#55277,#55278,#55279,#55280,#55281,#55282,#55283,#55284,#55285,#55286,#55287,
#55288,#55289,#55290,#55291,#55292,#55293,#55294,#55295,#55296,#55297,#55298,
#55299,#55300,#55301,#55302,#55303,#55304,#55305,#55306,#55307,#55308,#55309,
#55310,#55311,#55312,#55313,#55314,#55315,#55316,#55317,#55318,#55319,#55320,
#55321,#55322,#55323,#55324,#55325,#55326,#55327,#55328,#55329,#55330,#55331,
#55332,#55333,#55334,#55335,#55336,#55337,#55338,#55339,#55340,#55341,#55342,
#55343,#55344,#55345,#55346,#55347,#55348,#55349,#55350,#55351,#55352,#55353,
#55354,#55355,#55356,#55357,#55358,#55359,#55360,#55361,#55362,#55363,#55364,
#55365,#55366,#55367,#55368,#55369,#55370,#55371,#55372,#55373,#55374,#55375,
#55376,#55377,#55378,#55379,#55380,#55381,#55382,#55383,#55384,#55385,#55386,
#55387,#55388,#55389,#55390,#55391,#55392,#55393,#55394,#55395,#55396,#55397,
#55398,#55399,#55400,#55401,#55402,#55403,#55404,#55405,#55406,#55407,#55408,
#55409,#55410,#55411,#55412,#55413,#55414,#55415,#55416,#55417,#55418,#55419,
#55420,#55421,#55422,#55423,#55424,#55425,#55426,#55427,#55428,#55429,#55430,
#55431,#55432,#55433,#55434,#55435,#55436,#55437,#55438,#55439,#55440,#55441,
#55442,#55443,#55444,#55445,#55446,#55447,#55448,#55449,#55450,#55451,#55452,
#55453,#55454,#55455,#55456,#55457,#55458,#55459,#55460,#55461,#55462,#55463,
#55464,#55465,#55466,#55467,#55468,#55469,#55470,#55471,#55472,#55473,#55474,
#55475),.UNSPECIFIED.,.F.,.F.,(4,3,3,3,3,3,3,3,3,3,3,3,3,3,3,3,3,3,3,3,
3,3,3,3,3,3,3,3,3,3,3,3,3,3,3,3,3,3,3,3,3,3,3,3,3,3,3,3,3,3,3,3,3,3,3,3,
3,3,3,3,3,3,3,3,3,3,3,3,3,3,3,3,3,3,3,4),(32.5259719395726,32.6198747736003,
32.7140927372386,32.8084686989712,32.9031284200793,32.9905836306035,33.0791357826823,
33.1675731782046,33.2559196214019,33.3477169544862,33.4359610763914,33.5241917623266,
33.6124303810496,33.7006983018971,33.7890666025375,33.8774944136976,33.9660525497995,
33.9902982860763,34.0788504381557,34.1672878336786,34.2556342768766,34.3474316099607,
34.4356757318666,34.5239064178025,34.6121450365262,34.7004129573742,34.7887812580152,
34.877209069176,34.9657672052786,34.9900129415491,35.0785650936291,35.1670024891527,
35.2553489323512,35.347146265435,35.4353903873415,35.523621073278,35.6118596920023,
35.700127612851,35.7884959134927,35.876923724654,35.9654818607572,35.989727597022,
36.0782797491015,36.1667171446245,36.2550635878225,36.3468609209065,36.4351050428125,
36.5233357287484,36.6115743474721,36.6998422683203,36.7882105689614,36.8766383801223,
36.965196516225,36.9894422524948,37.0779944045744,37.1664318000975,37.2547782432956,
37.3465755763796,37.4348196982857,37.5230503842218,37.6112890029456,37.6995569237938,
37.787925224435,37.876353035596,37.9649111716988,37.9891569079676,38.0763924369636,
38.167988014092,38.2550056857047,38.3419692858987,38.4289013632082,38.5158244322685,
38.6027961903102,38.6897963120411,38.7768888180479,38.8091570539906),
 .UNSPECIFIED.);
#316=B_SPLINE_CURVE_WITH_KNOTS('',3,(#55477,#55478,#55479,#55480,#55481,
#55482,#55483,#55484,#55485,#55486,#55487),.UNSPECIFIED.,.F.,.F.,(4,1,1,
1,1,1,1,1,4),(38.8091570539906,38.9888715634404,39.9885862189133,40.9883008743861,
41.9880155298589,42.9877301853318,43.9874448408046,44.9871594962775,45.0923423611702),
 .UNSPECIFIED.);
#317=B_SPLINE_CURVE_WITH_KNOTS('',3,(#55489,#55490,#55491,#55492,#55493,
#55494,#55495,#55496,#55497,#55498),.UNSPECIFIED.,.F.,.F.,(4,1,1,1,1,1,
1,4),(45.0923423611702,45.9868741517503,46.9865888072231,47.986303462696,
48.9860181181688,49.9857327736416,50.9854474291144,51.3755276683498),
 .UNSPECIFIED.);
#318=B_SPLINE_CURVE_WITH_KNOTS('',3,(#55500,#55501,#55502,#55503,#55504,
#55505,#55506,#55507,#55508,#55509),.UNSPECIFIED.,.F.,.F.,(4,1,1,1,1,1,
1,4),(51.3755276683498,51.9851620845873,52.9848767400601,53.984591395533,
54.9843060510058,55.9840207064786,56.9837353619515,57.6587129755294),
 .UNSPECIFIED.);
#319=B_SPLINE_CURVE_WITH_KNOTS('',3,(#55511,#55512,#55513,#55514,#55515,
#55516,#55517,#55518,#55519,#55520),.UNSPECIFIED.,.F.,.F.,(4,1,1,1,1,1,
1,4),(57.6587129755294,57.9834500174243,58.9831646728971,59.98287932837,
60.9825939838428,61.9823086393156,62.9820232947885,63.9418930085214),
 .UNSPECIFIED.);
#320=B_SPLINE_CURVE_WITH_KNOTS('',3,(#55522,#55523,#55524,#55525,#55526,
#55527,#55528,#55529,#55530,#55531,#55532,#55533,#55534,#55535,#55536,#55537,
#55538,#55539,#55540,#55541,#55542,#55543,#55544,#55545,#55546,#55547,#55548,
#55549,#55550,#55551,#55552,#55553,#55554,#55555,#55556,#55557,#55558,#55559,
#55560,#55561,#55562,#55563,#55564,#55565,#55566,#55567,#55568,#55569,#55570,
#55571,#55572,#55573,#55574,#55575,#55576,#55577,#55578,#55579,#55580,#55581,
#55582,#55583,#55584,#55585,#55586,#55587,#55588,#55589,#55590,#55591,#55592,
#55593,#55594,#55595,#55596,#55597,#55598,#55599,#55600,#55601,#55602,#55603,
#55604,#55605,#55606,#55607,#55608,#55609,#55610,#55611,#55612,#55613,#55614,
#55615,#55616,#55617,#55618,#55619,#55620,#55621,#55622,#55623,#55624,#55625,
#55626,#55627,#55628,#55629,#55630,#55631,#55632,#55633,#55634,#55635,#55636,
#55637,#55638,#55639,#55640,#55641,#55642,#55643,#55644,#55645,#55646,#55647,
#55648,#55649,#55650,#55651,#55652,#55653,#55654,#55655,#55656,#55657,#55658,
#55659,#55660,#55661,#55662,#55663,#55664,#55665,#55666,#55667,#55668,#55669,
#55670,#55671,#55672,#55673,#55674,#55675,#55676,#55677,#55678,#55679,#55680,
#55681,#55682,#55683,#55684,#55685,#55686,#55687,#55688,#55689,#55690,#55691,
#55692,#55693,#55694,#55695,#55696,#55697,#55698,#55699,#55700,#55701,#55702,
#55703,#55704,#55705,#55706,#55707,#55708,#55709,#55710,#55711,#55712,#55713,
#55714,#55715,#55716,#55717,#55718,#55719,#55720,#55721,#55722,#55723,#55724,
#55725,#55726,#55727,#55728,#55729,#55730,#55731,#55732,#55733,#55734,#55735,
#55736,#55737,#55738,#55739,#55740,#55741,#55742,#55743,#55744,#55745,#55746,
#55747,#55748,#55749,#55750),.UNSPECIFIED.,.F.,.F.,(4,3,3,3,3,3,3,3,3,3,
3,3,3,3,3,3,3,3,3,3,3,3,3,3,3,3,3,3,3,3,3,3,3,3,3,3,3,3,3,3,3,3,3,3,3,3,
3,3,3,3,3,3,3,3,3,3,3,3,3,3,3,3,3,3,3,3,3,3,3,3,3,3,3,3,3,3,4),(63.941898282709,
63.9817379502613,64.0702901023407,64.1587274978637,64.2470739410617,64.3388712741458,
64.4271153960517,64.5153460819876,64.6035847007114,64.6918526215597,64.7802209222009,
64.8686487333618,64.9572068694644,64.9814526057341,65.0700047578135,65.1584421533364,
65.2467885965344,65.3385859296185,65.4268300515243,65.5150607374601,65.6032993561838,
65.6915672770317,65.7799355776727,65.8683633888335,65.956921524936,65.9811672612069,
66.0697194132867,66.1581568088099,66.2465032520082,66.3383005850922,66.4265447069984,
66.5147753929347,66.6030140116587,66.6912819325071,66.7796502331486,66.8680780443097,
66.9566361804127,66.9808819166798,67.0694340687594,67.1578714642826,67.2462179074807,
67.3380152405647,67.4262593624707,67.5144900484069,67.6027286671308,67.690996587979,
67.7793648886204,67.8677926997814,67.9563508358842,67.9805965721526,68.0691487242322,
68.1575861197554,68.2459325629534,68.3377298960374,68.4259740179435,68.5142047038796,
68.6024433226034,68.6907112434517,68.7790795440929,68.8675073552539,68.9560654913567,
68.9803112276255,69.0688633797051,69.1573007752283,69.2456472184266,69.3374445515105,
69.4256886734166,69.5139193593527,69.6021579780765,69.6904258989248,69.7787941995661,
69.867222010727,69.9557801468299,69.9800258830983,70.1025546974403,70.2168203982943,
70.2250835117824),.UNSPECIFIED.);
#321=B_SPLINE_CURVE_WITH_KNOTS('',3,(#55752,#55753,#55754,#55755,#55756,
#55757,#55758,#55759,#55760,#55761),.UNSPECIFIED.,.F.,.F.,(4,1,1,1,1,1,
1,4),(70.2250835898886,70.9797405385711,71.979455194044,72.9791698495168,
73.9788845049896,74.9785991604624,75.9783138159352,76.5082688970682),
 .UNSPECIFIED.);
#322=B_SPLINE_CURVE_WITH_KNOTS('',3,(#55763,#55764,#55765,#55766,#55767,
#55768,#55769,#55770,#55771,#55772),.UNSPECIFIED.,.F.,.F.,(4,1,1,1,1,1,
1,4),(76.5082688970682,76.9780284714081,77.9777431268809,78.9774577823538,
79.9771724378266,80.9768870932994,81.9766017487723,82.7914495005134),
 .UNSPECIFIED.);
#323=B_SPLINE_CURVE_WITH_KNOTS('',3,(#55774,#55775,#55776,#55777,#55778,
#55779,#55780,#55781,#55782,#55783,#55784,#55785,#55786,#55787,#55788,#55789,
#55790,#55791,#55792,#55793,#55794,#55795,#55796,#55797,#55798,#55799,#55800,
#55801,#55802,#55803,#55804,#55805,#55806,#55807,#55808,#55809,#55810,#55811,
#55812,#55813,#55814,#55815,#55816,#55817,#55818,#55819,#55820,#55821,#55822,
#55823,#55824,#55825,#55826,#55827,#55828,#55829,#55830,#55831,#55832,#55833,
#55834,#55835,#55836,#55837,#55838,#55839,#55840,#55841,#55842,#55843,#55844,
#55845,#55846,#55847,#55848,#55849,#55850,#55851,#55852,#55853,#55854,#55855,
#55856,#55857,#55858,#55859,#55860,#55861,#55862,#55863,#55864,#55865,#55866,
#55867,#55868,#55869,#55870,#55871,#55872,#55873,#55874,#55875,#55876,#55877,
#55878,#55879,#55880,#55881,#55882,#55883,#55884,#55885,#55886,#55887,#55888,
#55889,#55890,#55891,#55892,#55893,#55894,#55895,#55896,#55897,#55898,#55899,
#55900,#55901,#55902,#55903,#55904,#55905,#55906,#55907,#55908,#55909,#55910,
#55911,#55912,#55913,#55914,#55915,#55916,#55917,#55918,#55919,#55920,#55921,
#55922,#55923,#55924,#55925,#55926,#55927,#55928,#55929,#55930,#55931,#55932,
#55933,#55934,#55935,#55936,#55937,#55938,#55939,#55940,#55941,#55942,#55943,
#55944,#55945,#55946,#55947,#55948,#55949,#55950,#55951,#55952,#55953,#55954,
#55955,#55956,#55957,#55958,#55959,#55960,#55961,#55962,#55963,#55964,#55965,
#55966,#55967,#55968,#55969,#55970,#55971,#55972,#55973,#55974,#55975,#55976,
#55977,#55978,#55979,#55980,#55981,#55982,#55983,#55984,#55985,#55986,#55987,
#55988,#55989,#55990,#55991,#55992,#55993,#55994,#55995,#55996,#55997,#55998,
#55999),.UNSPECIFIED.,.F.,.F.,(4,3,3,3,3,3,3,3,3,3,3,3,3,3,3,3,3,3,3,3,
3,3,3,3,3,3,3,3,3,3,3,3,3,3,3,3,3,3,3,3,3,3,3,3,3,3,3,3,3,3,3,3,3,3,3,3,
3,3,3,3,3,3,3,3,3,3,3,3,3,3,3,3,3,3,3,4),(82.7914542042478,82.9239679358683,
82.9763164042451,83.0648685563247,83.1533059518479,83.2416523950459,83.3334497281299,
83.421693850036,83.5099245359721,83.5981631546961,83.6864310755445,83.7747993761859,
83.8632271873468,83.9517853234496,83.9760310597179,84.0645832117975,84.1530206073208,
84.2413670505189,84.3331643836029,84.4214085055091,84.5096391914452,84.5978778101692,
84.6861457310175,84.7745140316589,84.8629418428199,84.9514999789228,84.9757457151908,
85.0642978672704,85.1527352627935,85.2410817059916,85.3328790390756,85.4211231609817,
85.5093538469178,85.5975924656416,85.6858603864899,85.7742286871312,85.8626564982922,
85.9512146343949,85.9754603706636,86.0640125227432,86.1524499182664,86.2407963614645,
86.3325936945485,86.4208378164545,86.5090685023906,86.5973071211145,86.6855750419628,
86.7739433426041,86.8623711537651,86.9509292898679,86.9751750261364,87.063727178216,
87.1521645737392,87.2405110169374,87.3323083500214,87.4205524719275,87.5087831578636,
87.5970217765875,87.6852896974356,87.7736579980769,87.8620858092379,87.9506439453407,
87.9748896816092,88.0634418336888,88.151879229212,88.24022567241,88.332023005494,
88.4202671274001,88.5084978133362,88.5967364320601,88.6850043529082,88.7733726535495,
88.8618004647105,88.9503586008133,88.9746043370821,89.0746395114274),
 .UNSPECIFIED.);
#324=B_SPLINE_CURVE_WITH_KNOTS('',3,(#56001,#56002,#56003,#56004,#56005,
#56006,#56007,#56008,#56009,#56010),.UNSPECIFIED.,.F.,.F.,(4,1,1,1,1,1,
1,4),(89.0746484612627,89.9743189925549,90.9740336480277,91.9737483035006,
92.9734629589734,93.9731776144462,94.9728922699191,95.3578173614012),
 .UNSPECIFIED.);
#325=B_SPLINE_CURVE_WITH_KNOTS('',3,(#56012,#56013,#56014,#56015,#56016,
#56017,#56018,#56019,#56020,#56021,#56022,#56023,#56024,#56025,#56026,#56027,
#56028,#56029,#56030,#56031,#56032,#56033,#56034,#56035,#56036,#56037,#56038,
#56039,#56040,#56041,#56042,#56043,#56044,#56045,#56046,#56047,#56048,#56049,
#56050,#56051,#56052,#56053,#56054,#56055,#56056,#56057,#56058,#56059,#56060,
#56061,#56062,#56063,#56064,#56065,#56066,#56067,#56068,#56069,#56070,#56071,
#56072,#56073,#56074,#56075,#56076,#56077,#56078,#56079,#56080,#56081,#56082,
#56083,#56084,#56085,#56086,#56087,#56088,#56089,#56090,#56091,#56092,#56093,
#56094,#56095,#56096,#56097,#56098,#56099,#56100,#56101,#56102,#56103,#56104,
#56105,#56106,#56107,#56108,#56109,#56110,#56111,#56112,#56113,#56114,#56115,
#56116,#56117,#56118,#56119,#56120,#56121,#56122,#56123,#56124,#56125,#56126,
#56127,#56128,#56129,#56130,#56131,#56132,#56133,#56134,#56135,#56136,#56137,
#56138,#56139,#56140,#56141,#56142,#56143,#56144,#56145,#56146,#56147,#56148,
#56149,#56150,#56151,#56152,#56153,#56154,#56155,#56156,#56157,#56158,#56159,
#56160,#56161,#56162,#56163,#56164,#56165,#56166,#56167,#56168,#56169,#56170,
#56171,#56172,#56173,#56174,#56175,#56176,#56177,#56178,#56179,#56180,#56181,
#56182,#56183,#56184,#56185,#56186,#56187,#56188,#56189,#56190,#56191,#56192,
#56193,#56194,#56195,#56196,#56197,#56198,#56199,#56200,#56201,#56202,#56203,
#56204,#56205,#56206,#56207,#56208,#56209,#56210,#56211,#56212,#56213,#56214,
#56215,#56216,#56217,#56218,#56219,#56220,#56221,#56222,#56223,#56224,#56225,
#56226,#56227,#56228,#56229,#56230,#56231,#56232,#56233,#56234,#56235,#56236,
#56237),.UNSPECIFIED.,.F.,.F.,(4,3,3,3,3,3,3,3,3,3,3,3,3,3,3,3,3,3,3,3,
3,3,3,3,3,3,3,3,3,3,3,3,3,3,3,3,3,3,3,3,3,3,3,3,3,3,3,3,3,3,3,3,3,3,3,3,
3,3,3,3,3,3,3,3,3,3,3,3,3,3,3,3,3,3,3,4),(95.3578248186069,95.4469228467246,
95.5360360002453,95.6251842465887,95.7144518819726,95.8037810607741,95.8932749187053,
95.9726069253919,96.0611590774715,96.1495964729946,96.2379429161925,96.3297402492765,
96.4179843711827,96.5062150571188,96.5944536758426,96.6827215966912,96.7710898973325,
96.8595177084935,96.9480758445963,96.9723215808647,97.0608737329443,97.1493111284676,
97.2376575716657,97.3294549047497,97.4176990266558,97.505929712592,97.5941683313159,
97.6824362521645,97.7708045528058,97.8592323639669,97.9477905000696,97.9720362363376,
98.0605883884171,98.1490257839403,98.2373722271387,98.3291695602226,98.4174136821287,
98.5056443680648,98.5938829867886,98.6821509076364,98.7705192082777,98.8589470194386,
98.9475051555416,98.9717508918104,99.0603030438901,99.1487404394132,99.2370868826112,
99.3288842156952,99.4171283376014,99.5053590235375,99.5935976422613,99.6818655631093,
99.7702338637505,99.8586616749113,99.947219811014,99.9714655472833,100.060017699363,
100.148455094886,100.236801538084,100.328598871168,100.416842993074,100.50507367901,
100.593312297734,100.681580218582,100.769948519224,100.858376330385,100.946934466487,
100.971180202756,101.05961993014,101.147948157046,101.236186505253,101.324356520768,
101.412486320201,101.500591756939,101.58871623251,101.641010125787),
 .UNSPECIFIED.);
#326=B_SPLINE_CURVE_WITH_KNOTS('',3,(#56239,#56240,#56241,#56242,#56243,
#56244,#56245,#56246,#56247,#56248),.UNSPECIFIED.,.F.,.F.,(4,1,1,1,1,1,
1,4),(101.641017304817,101.970894858229,102.970609513702,103.970324169175,
104.970038824647,105.96975348012,106.969468135593,107.924195432966),
 .UNSPECIFIED.);
#327=B_SPLINE_CURVE_WITH_KNOTS('',3,(#56250,#56251,#56252,#56253,#56254,
#56255,#56256,#56257,#56258,#56259,#56260,#56261),.UNSPECIFIED.,.F.,.F.,
(4,2,1,1,1,1,1,1,4),(107.924195432966,107.969182791066,108.968897446539,
109.968612102012,110.968326757484,111.968041412957,112.96775606843,113.967470723903,
114.207380740146),.UNSPECIFIED.);
#328=B_SPLINE_CURVE_WITH_KNOTS('',3,(#56263,#56264,#56265,#56266,#56267,
#56268,#56269,#56270,#56271,#56272),.UNSPECIFIED.,.F.,.F.,(4,1,1,1,1,1,
1,4),(114.207380740146,114.967185379376,115.966900034849,116.966614690321,
117.966329345794,118.966044001267,119.96575865674,120.490566047325),
 .UNSPECIFIED.);
#329=B_SPLINE_CURVE_WITH_KNOTS('',3,(#56274,#56275,#56276,#56277,#56278,
#56279,#56280,#56281,#56282,#56283),.UNSPECIFIED.,.F.,.F.,(4,1,1,1,1,1,
1,4),(120.490566047325,120.965473312213,121.965187967686,122.964902623158,
123.964617278631,124.964331934104,125.964046589577,126.773747127373),
 .UNSPECIFIED.);
#330=B_SPLINE_CURVE_WITH_KNOTS('',3,(#56285,#56286,#56287,#56288,#56289,
#56290,#56291,#56292,#56293,#56294,#56295,#56296,#56297,#56298,#56299,#56300,
#56301,#56302,#56303,#56304,#56305,#56306,#56307,#56308,#56309,#56310,#56311,
#56312,#56313,#56314,#56315,#56316,#56317,#56318,#56319,#56320,#56321,#56322,
#56323,#56324,#56325,#56326,#56327,#56328,#56329,#56330,#56331,#56332,#56333,
#56334,#56335,#56336,#56337,#56338,#56339,#56340,#56341,#56342,#56343,#56344,
#56345,#56346,#56347,#56348,#56349,#56350,#56351,#56352,#56353,#56354,#56355,
#56356,#56357,#56358,#56359,#56360,#56361,#56362,#56363,#56364,#56365,#56366,
#56367,#56368,#56369,#56370,#56371,#56372,#56373,#56374,#56375,#56376,#56377,
#56378,#56379,#56380,#56381,#56382,#56383,#56384,#56385,#56386,#56387,#56388,
#56389,#56390,#56391,#56392,#56393,#56394,#56395,#56396,#56397,#56398,#56399,
#56400,#56401,#56402,#56403,#56404,#56405,#56406,#56407,#56408,#56409,#56410,
#56411,#56412,#56413,#56414,#56415,#56416,#56417,#56418,#56419,#56420,#56421,
#56422,#56423,#56424,#56425,#56426,#56427,#56428,#56429,#56430,#56431,#56432,
#56433,#56434,#56435,#56436,#56437,#56438,#56439,#56440,#56441,#56442,#56443,
#56444,#56445,#56446,#56447,#56448,#56449,#56450,#56451,#56452,#56453,#56454,
#56455,#56456,#56457,#56458,#56459,#56460,#56461,#56462,#56463,#56464,#56465,
#56466,#56467,#56468,#56469,#56470,#56471,#56472,#56473,#56474,#56475,#56476,
#56477,#56478,#56479,#56480,#56481,#56482,#56483,#56484,#56485,#56486,#56487,
#56488,#56489,#56490,#56491,#56492,#56493,#56494,#56495,#56496,#56497,#56498,
#56499,#56500,#56501,#56502,#56503,#56504,#56505,#56506,#56507,#56508,#56509,
#56510),.UNSPECIFIED.,.F.,.F.,(4,3,3,3,3,3,3,3,3,3,3,3,3,3,3,3,3,3,3,3,
3,3,3,3,3,3,3,3,3,3,3,3,3,3,3,3,3,3,3,3,3,3,3,3,3,3,3,3,3,3,3,3,3,3,3,3,
3,3,3,3,3,3,3,3,3,3,3,3,3,3,3,3,3,3,3,4),(126.773751354505,126.904300810836,
126.96376124505,127.05231339713,127.140750792653,127.229097235851,127.320894568935,
127.409138690841,127.497369376777,127.5856079955,127.673875916349,127.76224421699,
127.850672028151,127.939230164253,127.963475900523,128.052028052602,128.140465448125,
128.228811891323,128.320609224407,128.408853346313,128.497084032249,128.585322650973,
128.673590571821,128.761958872462,128.850386683623,128.938944819725,128.963190555995,
129.051742708075,129.140180103598,129.228526546796,129.32032387988,129.408568001786,
129.496798687722,129.585037306446,129.673305227294,129.761673527936,129.850101339097,
129.9386594752,129.962905211468,130.051457363548,130.139894759071,130.228241202269,
130.320038535353,130.408282657259,130.496513343196,130.58475196192,130.673019882768,
130.76138818341,130.849815994571,130.938374130674,130.962619866941,131.051172019021,
131.139609414544,131.227955857742,131.319753190826,131.407997312732,131.496227998668,
131.584466617392,131.67273453824,131.761102838881,131.849530650042,131.938088786145,
131.962334522414,132.050886674494,132.139324070017,132.227670513215,132.319467846299,
132.407711968205,132.495942654141,132.584181272865,132.672449193713,132.760817494355,
132.849245305516,132.937803441618,132.962049177887,133.056936661685),
 .UNSPECIFIED.);
#331=B_SPLINE_CURVE_WITH_KNOTS('',3,(#56512,#56513,#56514,#56515,#56516,
#56517,#56518,#56519,#56520,#56521),.UNSPECIFIED.,.F.,.F.,(4,1,1,1,1,1,
1,4),(133.056945554371,133.96176383336,134.961478488832,135.961193144305,
136.960907799778,137.960622455251,138.960337110724,139.340114405502),
 .UNSPECIFIED.);
#332=B_SPLINE_CURVE_WITH_KNOTS('',3,(#56523,#56524,#56525,#56526,#56527,
#56528,#56529,#56530,#56531,#56532,#56533,#56534,#56535,#56536,#56537,#56538,
#56539,#56540,#56541,#56542,#56543,#56544,#56545,#56546,#56547,#56548,#56549,
#56550,#56551,#56552,#56553,#56554,#56555,#56556,#56557,#56558,#56559,#56560,
#56561,#56562,#56563,#56564,#56565,#56566,#56567,#56568,#56569,#56570,#56571,
#56572,#56573,#56574,#56575,#56576,#56577,#56578,#56579,#56580,#56581,#56582,
#56583,#56584,#56585,#56586,#56587,#56588,#56589,#56590,#56591,#56592,#56593,
#56594,#56595,#56596,#56597,#56598,#56599,#56600,#56601,#56602,#56603,#56604,
#56605,#56606,#56607,#56608,#56609,#56610,#56611,#56612,#56613,#56614,#56615,
#56616,#56617,#56618,#56619,#56620,#56621,#56622,#56623,#56624,#56625,#56626,
#56627,#56628,#56629,#56630,#56631,#56632,#56633,#56634,#56635,#56636,#56637,
#56638,#56639,#56640,#56641,#56642,#56643,#56644,#56645,#56646,#56647,#56648,
#56649,#56650,#56651,#56652,#56653,#56654,#56655,#56656,#56657,#56658,#56659,
#56660,#56661,#56662,#56663,#56664,#56665,#56666,#56667,#56668,#56669,#56670,
#56671,#56672,#56673,#56674,#56675,#56676,#56677,#56678,#56679,#56680,#56681,
#56682,#56683,#56684,#56685,#56686,#56687,#56688,#56689,#56690,#56691,#56692,
#56693,#56694,#56695,#56696,#56697,#56698,#56699,#56700,#56701,#56702,#56703,
#56704,#56705,#56706,#56707,#56708,#56709,#56710,#56711,#56712,#56713,#56714,
#56715,#56716,#56717,#56718,#56719,#56720,#56721,#56722,#56723,#56724,#56725,
#56726,#56727,#56728,#56729,#56730,#56731,#56732,#56733,#56734,#56735,#56736,
#56737,#56738,#56739,#56740,#56741,#56742,#56743,#56744,#56745,#56746,#56747,
#56748),.UNSPECIFIED.,.F.,.F.,(4,3,3,3,3,3,3,3,3,3,3,3,3,3,3,3,3,3,3,3,
3,3,3,3,3,3,3,3,3,3,3,3,3,3,3,3,3,3,3,3,3,3,3,3,3,3,3,3,3,3,3,3,3,3,3,3,
3,3,3,3,3,3,3,3,3,3,3,3,3,3,3,3,3,3,3,4),(139.340121968864,139.429114310097,
139.51811844929,139.607154538274,139.696307192852,139.785518959188,139.874895927097,
139.960051766197,140.048603918276,140.137041313799,140.225387756997,140.317185090081,
140.405429211987,140.493659897922,140.581898516646,140.670166437494,140.758534738135,
140.846962549295,140.935520685398,140.959766421669,141.048318573749,141.136755969272,
141.22510241247,141.316899745554,141.40514386746,141.493374553396,141.58161317212,
141.669881092968,141.758249393609,141.84667720477,141.935235340873,141.959481077142,
142.048033229222,142.136470624745,142.224817067943,142.316614401027,142.404858522933,
142.49308920887,142.581327827594,142.669595748442,142.757964049084,142.846391860245,
142.934949996348,142.959195732615,143.047747884695,143.136185280218,143.224531723416,
143.3163290565,143.404573178406,143.492803864342,143.581042483066,143.669310403914,
143.757678704556,143.846106515716,143.934664651819,143.958910388088,144.047462540168,
144.135899935691,144.224246378889,144.316043711973,144.404287833879,144.492518519815,
144.580757138539,144.669025059388,144.757393360029,144.84582117119,144.934379307293,
144.958625043561,145.047148680272,145.135560075733,145.223880758912,145.312132182873,
145.400341173324,145.48852490424,145.576724249091,145.623307276044),
 .UNSPECIFIED.);
#333=B_SPLINE_CURVE_WITH_KNOTS('',3,(#56750,#56751,#56752,#56753,#56754,
#56755,#56756,#56757,#56758,#56759),.UNSPECIFIED.,.F.,.F.,(4,1,1,1,1,1,
1,4),(145.623314614479,145.958339699034,146.958054354506,147.957769009979,
148.957483665452,149.957198320925,150.956912976398,151.906492583223),
 .UNSPECIFIED.);
#334=B_SPLINE_CURVE_WITH_KNOTS('',3,(#56761,#56762,#56763,#56764,#56765,
#56766,#56767,#56768,#56769,#56770,#56771,#56772),.UNSPECIFIED.,.F.,.F.,
(4,2,1,1,1,1,1,1,4),(151.906492583223,151.956627631871,152.956342287343,
153.956056942816,154.955771598289,155.955486253762,156.955200909235,157.954915564708,
158.189677890403),.UNSPECIFIED.);
#335=B_SPLINE_CURVE_WITH_KNOTS('',3,(#56774,#56775,#56776,#56777,#56778,
#56779,#56780,#56781,#56782,#56783),.UNSPECIFIED.,.F.,.F.,(4,1,1,1,1,1,
1,4),(158.189677890403,158.95463022018,159.954344875653,160.954059531126,
161.953774186599,162.953488842072,163.953203497545,164.472863197582),
 .UNSPECIFIED.);
#336=B_SPLINE_CURVE_WITH_KNOTS('',3,(#56785,#56786,#56787,#56788,#56789,
#56790,#56791,#56792,#56793,#56794),.UNSPECIFIED.,.F.,.F.,(4,1,1,1,1,1,
1,4),(164.472863197582,164.952918153017,165.95263280849,166.952347463963,
167.952062119436,168.951776774909,169.951491430381,170.756044766746),
 .UNSPECIFIED.);
#337=B_SPLINE_CURVE_WITH_KNOTS('',3,(#56796,#56797,#56798,#56799,#56800,
#56801,#56802,#56803,#56804,#56805,#56806,#56807,#56808,#56809,#56810,#56811,
#56812,#56813,#56814,#56815,#56816,#56817,#56818,#56819,#56820,#56821,#56822,
#56823,#56824,#56825,#56826,#56827,#56828,#56829,#56830,#56831,#56832,#56833,
#56834,#56835,#56836,#56837,#56838,#56839,#56840,#56841,#56842,#56843,#56844,
#56845,#56846,#56847,#56848,#56849,#56850,#56851,#56852,#56853,#56854,#56855,
#56856,#56857,#56858,#56859,#56860,#56861,#56862,#56863,#56864,#56865,#56866,
#56867,#56868,#56869,#56870,#56871,#56872,#56873,#56874,#56875,#56876,#56877,
#56878,#56879,#56880,#56881,#56882,#56883,#56884,#56885,#56886,#56887,#56888,
#56889,#56890,#56891,#56892,#56893,#56894,#56895,#56896,#56897,#56898,#56899,
#56900,#56901,#56902,#56903,#56904,#56905,#56906,#56907,#56908,#56909,#56910,
#56911,#56912,#56913,#56914,#56915,#56916,#56917,#56918,#56919,#56920,#56921,
#56922,#56923,#56924,#56925,#56926,#56927,#56928,#56929,#56930,#56931,#56932,
#56933,#56934,#56935,#56936,#56937,#56938,#56939,#56940,#56941,#56942,#56943,
#56944,#56945,#56946,#56947,#56948,#56949,#56950,#56951,#56952,#56953,#56954,
#56955,#56956,#56957,#56958,#56959,#56960,#56961,#56962,#56963,#56964,#56965,
#56966,#56967,#56968,#56969,#56970,#56971,#56972,#56973,#56974,#56975,#56976,
#56977,#56978,#56979,#56980,#56981,#56982,#56983,#56984,#56985,#56986,#56987,
#56988,#56989,#56990,#56991,#56992,#56993,#56994,#56995,#56996,#56997,#56998,
#56999,#57000,#57001,#57002,#57003,#57004,#57005,#57006,#57007,#57008,#57009,
#57010,#57011,#57012,#57013,#57014,#57015,#57016,#57017,#57018,#57019,#57020,
#57021),.UNSPECIFIED.,.F.,.F.,(4,3,3,3,3,3,3,3,3,3,3,3,3,3,3,3,3,3,3,3,
3,3,3,3,3,3,3,3,3,3,3,3,3,3,3,3,3,3,3,3,3,3,3,3,3,3,3,3,3,3,3,3,3,3,3,3,
3,3,3,3,3,3,3,3,3,3,3,3,3,3,3,3,3,3,3,4),(170.756048504762,170.884766228992,
170.951206085854,171.039758237934,171.128195633458,171.216542076657,171.308339409741,
171.396583531648,171.484814217584,171.573052836309,171.661320757158,171.7496890578,
171.838116868962,171.926675005065,171.950920741327,172.039472893407,172.12791028893,
172.216256732128,172.308054065212,172.396298187118,172.484528873054,172.572767491778,
172.661035412626,172.749403713267,172.837831524428,172.926389660531,172.9506353968,
173.03918754888,173.127624944403,173.215971387601,173.307768720685,173.396012842591,
173.484243528527,173.57248214725,173.660750068099,173.74911836874,173.837546179901,
173.926104316003,173.950350052273,174.038902204353,174.127339599876,174.215686043074,
174.307483376158,174.395727498064,174.483958184,174.572196802724,174.660464723573,
174.748833024214,174.837260835375,174.925818971478,174.950064707746,175.038616859826,
175.127054255349,175.215400698547,175.307198031631,175.395442153537,175.483672839474,
175.571911458198,175.660179379046,175.748547679687,175.836975490849,175.925533626951,
175.949779363219,176.038331515298,176.126768910822,176.21511535402,176.306912687103,
176.395156809009,176.483387494945,176.571626113669,176.659894034517,176.748262335158,
176.836690146319,176.925248282422,176.949494018691,177.039233811941),
 .UNSPECIFIED.);
#338=B_SPLINE_CURVE_WITH_KNOTS('',3,(#57023,#57024,#57025,#57026,#57027,
#57028,#57029,#57030,#57031,#57032),.UNSPECIFIED.,.F.,.F.,(4,1,1,1,1,1,
1,4),(177.039242603138,177.949208674164,178.948923329637,179.94863798511,
180.948352640583,181.948067296056,182.947781951528,183.322411476105),
 .UNSPECIFIED.);
#339=B_SPLINE_CURVE_WITH_KNOTS('',3,(#57034,#57035,#57036,#57037,#57038,
#57039,#57040,#57041,#57042,#57043,#57044,#57045,#57046,#57047,#57048,#57049,
#57050,#57051,#57052,#57053,#57054,#57055,#57056,#57057,#57058,#57059,#57060,
#57061,#57062,#57063,#57064,#57065,#57066,#57067,#57068,#57069,#57070,#57071,
#57072,#57073,#57074,#57075,#57076,#57077,#57078,#57079,#57080,#57081,#57082,
#57083,#57084,#57085,#57086,#57087,#57088,#57089,#57090,#57091,#57092,#57093,
#57094,#57095,#57096,#57097,#57098,#57099,#57100,#57101,#57102,#57103,#57104,
#57105,#57106,#57107,#57108,#57109,#57110,#57111,#57112,#57113,#57114,#57115,
#57116,#57117,#57118,#57119,#57120,#57121,#57122,#57123,#57124,#57125,#57126,
#57127,#57128,#57129,#57130,#57131,#57132,#57133,#57134,#57135,#57136,#57137,
#57138,#57139,#57140,#57141,#57142,#57143,#57144,#57145,#57146,#57147,#57148,
#57149,#57150,#57151,#57152,#57153,#57154,#57155,#57156,#57157,#57158,#57159,
#57160,#57161,#57162,#57163,#57164,#57165,#57166,#57167,#57168,#57169,#57170,
#57171,#57172,#57173,#57174,#57175,#57176,#57177,#57178,#57179,#57180,#57181,
#57182,#57183,#57184,#57185,#57186,#57187,#57188,#57189,#57190,#57191,#57192,
#57193,#57194,#57195,#57196,#57197,#57198,#57199,#57200,#57201,#57202,#57203,
#57204,#57205,#57206,#57207,#57208,#57209,#57210,#57211,#57212,#57213,#57214,
#57215,#57216,#57217,#57218,#57219,#57220,#57221,#57222,#57223,#57224,#57225,
#57226,#57227,#57228,#57229,#57230,#57231,#57232,#57233,#57234,#57235,#57236,
#57237,#57238,#57239,#57240,#57241,#57242,#57243,#57244,#57245,#57246,#57247,
#57248,#57249,#57250,#57251,#57252,#57253,#57254,#57255,#57256,#57257,#57258,
#57259),.UNSPECIFIED.,.F.,.F.,(4,3,3,3,3,3,3,3,3,3,3,3,3,3,3,3,3,3,3,3,
3,3,3,3,3,3,3,3,3,3,3,3,3,3,3,3,3,3,3,3,3,3,3,3,3,3,3,3,3,3,3,3,3,3,3,3,
3,3,3,3,3,3,3,3,3,3,3,3,3,3,3,3,3,3,3,4),(183.322419119121,183.411309023726,
183.500207494653,183.589134856038,183.678725293779,183.767823606447,183.857660106724,
183.947496607001,184.036048759081,184.124486154604,184.212832597802,184.304629930886,
184.392874052792,184.481104738728,184.569343357452,184.6576112783,184.745979578942,
184.834407390103,184.922965526206,184.947211262474,185.035763414554,185.124200810077,
185.212547253275,185.304344586359,185.392588708265,185.480819394201,185.569058012925,
185.657325933774,185.745694234415,185.834122045576,185.922680181679,185.946925917947,
186.035478070027,186.12391546555,186.212261908748,186.304059241832,186.392303363738,
186.480534049674,186.568772668398,186.657040589246,186.745408889888,186.833836701049,
186.922394837152,186.94664057342,187.0351927255,187.123630121023,187.211976564221,
187.303773897305,187.392018019211,187.480248705148,187.568487323872,187.65675524472,
187.745123545362,187.833551356523,187.922109492626,187.946355228893,188.034907380972,
188.123344776495,188.211691219693,188.303488552777,188.391732674683,188.479963360619,
188.568201979342,188.656469900191,188.744838200832,188.833266011993,188.921824148096,
188.946069884365,189.034680468163,189.12317803393,189.211584011424,189.299919754286,
189.388210799519,189.476475634494,189.564752692411,189.605604426301),
 .UNSPECIFIED.);
#340=B_SPLINE_CURVE_WITH_KNOTS('',3,(#57261,#57262,#57263,#57264,#57265,
#57266,#57267,#57268,#57269,#57270),.UNSPECIFIED.,.F.,.F.,(4,1,1,1,1,1,
1,4),(189.605611896825,189.945784539838,190.945499195311,191.945213850784,
192.944928506257,193.94464316173,194.944357817202,195.88878973348),
 .UNSPECIFIED.);
#341=B_SPLINE_CURVE_WITH_KNOTS('',3,(#57272,#57273,#57274,#57275,#57276,
#57277,#57278,#57279,#57280,#57281,#57282),.UNSPECIFIED.,.F.,.F.,(4,1,1,
1,1,1,1,1,4),(195.88878973348,195.944072472675,196.943787128148,197.943501783621,
198.943216439094,199.942931094567,200.942645750039,201.942360405512,202.17197504066),
 .UNSPECIFIED.);
#342=B_SPLINE_CURVE_WITH_KNOTS('',3,(#57284,#57285,#57286,#57287,#57288,
#57289,#57290,#57291,#57292,#57293),.UNSPECIFIED.,.F.,.F.,(4,1,1,1,1,1,
1,4),(202.17197504066,202.942075060985,203.941789716458,204.941504371931,
205.941219027403,206.940933682876,207.940648338349,208.455160347839),
 .UNSPECIFIED.);
#343=B_SPLINE_CURVE_WITH_KNOTS('',3,(#57295,#57296,#57297,#57298,#57299,
#57300,#57301,#57302,#57303,#57304),.UNSPECIFIED.,.F.,.F.,(4,1,1,1,1,1,
1,4),(208.455160347839,208.940362993822,209.940077649295,210.939792304768,
211.939506960241,212.939221615713,213.938936271186,214.738345655019),
 .UNSPECIFIED.);
#344=B_SPLINE_CURVE_WITH_KNOTS('',3,(#57306,#57307,#57308,#57309,#57310,
#57311,#57312,#57313,#57314,#57315,#57316),.UNSPECIFIED.,.F.,.F.,(4,1,1,
1,1,1,1,1,4),(214.738345655019,214.938650926659,215.938365582132,216.938080237605,
217.937794893078,218.93750954855,219.937224204023,220.936938859496,221.021530962198),
 .UNSPECIFIED.);
#345=B_SPLINE_CURVE_WITH_KNOTS('',3,(#57318,#57319,#57320,#57321,#57322,
#57323,#57324,#57325,#57326,#57327),.UNSPECIFIED.,.F.,.F.,(4,1,1,1,1,1,
1,4),(221.021530962198,221.936653514969,222.936368170442,223.936082825914,
224.935797481387,225.93551213686,226.935226792333,227.304716269378),
 .UNSPECIFIED.);
#346=B_SPLINE_CURVE_WITH_KNOTS('',3,(#57329,#57330,#57331,#57332,#57333,
#57334,#57335,#57336,#57337,#57338),.UNSPECIFIED.,.F.,.F.,(4,1,1,1,1,1,
1,4),(227.304716269378,227.934941447806,228.934656103279,229.934370758752,
230.934085414224,231.933800069697,232.93351472517,233.587901576558),
 .UNSPECIFIED.);
#347=B_SPLINE_CURVE_WITH_KNOTS('',3,(#57340,#57341,#57342,#57343,#57344,
#57345,#57346,#57347,#57348,#57349,#57350,#57351,#57352,#57353,#57354,#57355,
#57356,#57357,#57358,#57359,#57360,#57361,#57362,#57363,#57364,#57365,#57366,
#57367,#57368,#57369,#57370,#57371,#57372,#57373,#57374,#57375,#57376,#57377,
#57378,#57379,#57380,#57381,#57382,#57383,#57384,#57385,#57386,#57387,#57388,
#57389,#57390,#57391,#57392,#57393,#57394,#57395,#57396,#57397,#57398,#57399,
#57400,#57401,#57402,#57403,#57404,#57405,#57406,#57407,#57408,#57409,#57410,
#57411,#57412,#57413,#57414,#57415,#57416,#57417,#57418,#57419,#57420,#57421,
#57422,#57423,#57424,#57425,#57426,#57427,#57428,#57429,#57430,#57431,#57432,
#57433,#57434,#57435,#57436,#57437,#57438,#57439,#57440,#57441,#57442,#57443,
#57444,#57445,#57446,#57447,#57448,#57449,#57450,#57451,#57452,#57453,#57454,
#57455,#57456,#57457,#57458,#57459,#57460,#57461,#57462,#57463,#57464,#57465,
#57466,#57467,#57468,#57469,#57470,#57471,#57472,#57473,#57474,#57475,#57476,
#57477,#57478,#57479,#57480,#57481,#57482,#57483,#57484,#57485,#57486,#57487,
#57488,#57489,#57490,#57491,#57492,#57493,#57494,#57495,#57496,#57497,#57498,
#57499,#57500,#57501,#57502,#57503,#57504,#57505,#57506,#57507,#57508,#57509,
#57510,#57511,#57512,#57513,#57514,#57515,#57516,#57517,#57518,#57519,#57520,
#57521,#57522,#57523,#57524,#57525,#57526,#57527,#57528,#57529,#57530,#57531,
#57532,#57533,#57534,#57535,#57536,#57537,#57538,#57539,#57540,#57541,#57542,
#57543,#57544,#57545,#57546,#57547,#57548,#57549,#57550,#57551,#57552,#57553,
#57554,#57555,#57556,#57557,#57558,#57559,#57560,#57561,#57562,#57563,#57564,
#57565),.UNSPECIFIED.,.F.,.F.,(4,3,3,3,3,3,3,3,3,3,3,3,3,3,3,3,3,3,3,3,
3,3,3,3,3,3,3,3,3,3,3,3,3,3,3,3,3,3,3,3,3,3,3,3,3,3,3,3,3,3,3,3,3,3,3,3,
3,3,3,3,3,3,3,3,3,3,3,3,3,3,3,3,3,3,3,4),(233.587901819524,233.689634913313,
233.791928180161,233.89488361089,233.933229380643,234.021781532723,234.110218928246,
234.198565371445,234.290362704529,234.378606826435,234.466837512371,234.555076131095,
234.643344051944,234.731712352586,234.820140163747,234.90869829985,234.932944036116,
235.021496188196,235.109933583719,235.198280026917,235.290077360001,235.378321481908,
235.466552167844,235.554790786568,235.643058707416,235.731427008058,235.819854819219,
235.908412955322,235.932658691589,236.021210843668,236.109648239191,236.197994682389,
236.289792015473,236.378036137379,236.466266823315,236.554505442038,236.642773362886,
236.731141663528,236.819569474688,236.908127610791,236.932373347061,237.020925499141,
237.109362894664,237.197709337862,237.289506670946,237.377750792852,237.465981478788,
237.554220097512,237.64248801836,237.730856319001,237.819284130162,237.907842266265,
237.932088002534,238.020640154614,238.109077550137,238.197423993335,238.289221326419,
238.377465448326,238.465696134262,238.553934752986,238.642202673834,238.730570974476,
238.818998785637,238.90755692174,238.931802658007,239.019567715922,239.107218672699,
239.194780175945,239.282278390013,239.369743686316,239.457198190576,239.544664015338,
239.632214924191,239.719810741112,239.807540789698,239.871086883737),
 .UNSPECIFIED.);
#348=B_SPLINE_CURVE_WITH_KNOTS('',3,(#57567,#57568,#57569,#57570,#57571,
#57572,#57573,#57574,#57575,#57576,#57577,#57578),.UNSPECIFIED.,.F.,.F.,
(4,2,1,1,1,1,1,1,4),(239.871086883737,239.93151731348,240.931231968953,
241.930946624426,242.930661279898,243.930375935371,244.930090590844,245.929805246317,
246.154272190917),.UNSPECIFIED.);
#349=B_SPLINE_CURVE_WITH_KNOTS('',3,(#57580,#57581,#57582,#57583,#57584,
#57585,#57586,#57587,#57588,#57589,#57590,#57591,#57592,#57593,#57594,#57595,
#57596,#57597,#57598,#57599,#57600,#57601,#57602,#57603,#57604,#57605,#57606,
#57607,#57608,#57609,#57610,#57611,#57612,#57613,#57614,#57615,#57616,#57617,
#57618,#57619,#57620,#57621,#57622,#57623,#57624,#57625,#57626,#57627,#57628,
#57629,#57630,#57631,#57632,#57633,#57634,#57635,#57636,#57637,#57638,#57639,
#57640,#57641,#57642,#57643,#57644,#57645,#57646,#57647,#57648,#57649,#57650,
#57651,#57652,#57653,#57654,#57655,#57656,#57657,#57658,#57659,#57660,#57661,
#57662,#57663,#57664,#57665,#57666,#57667,#57668,#57669,#57670,#57671,#57672,
#57673,#57674,#57675,#57676,#57677,#57678,#57679,#57680,#57681,#57682,#57683,
#57684,#57685,#57686,#57687,#57688,#57689,#57690,#57691,#57692,#57693,#57694,
#57695,#57696,#57697,#57698,#57699,#57700,#57701,#57702,#57703,#57704,#57705,
#57706,#57707,#57708,#57709,#57710,#57711,#57712,#57713,#57714,#57715,#57716,
#57717,#57718,#57719,#57720,#57721,#57722,#57723,#57724,#57725,#57726,#57727,
#57728,#57729,#57730,#57731,#57732,#57733,#57734,#57735,#57736,#57737,#57738,
#57739,#57740,#57741,#57742,#57743,#57744,#57745,#57746,#57747,#57748,#57749,
#57750,#57751,#57752,#57753,#57754,#57755,#57756,#57757,#57758,#57759,#57760,
#57761,#57762,#57763,#57764,#57765,#57766,#57767,#57768,#57769,#57770,#57771,
#57772,#57773,#57774,#57775,#57776,#57777,#57778,#57779,#57780,#57781,#57782,
#57783,#57784,#57785,#57786,#57787,#57788,#57789,#57790,#57791,#57792,#57793,
#57794,#57795,#57796,#57797,#57798,#57799,#57800,#57801,#57802,#57803,#57804,
#57805),.UNSPECIFIED.,.F.,.F.,(4,3,3,3,3,3,3,3,3,3,3,3,3,3,3,3,3,3,3,3,
3,3,3,3,3,3,3,3,3,3,3,3,3,3,3,3,3,3,3,3,3,3,3,3,3,3,3,3,3,3,3,3,3,3,3,3,
3,3,3,3,3,3,3,3,3,3,3,3,3,3,3,3,3,3,3,4),(246.154272190917,246.241451698402,
246.328564152085,246.415641150959,246.502705121084,246.58977847341,246.676938547938,
246.764142193271,246.851488540128,246.92951990179,247.01807205387,247.106509449393,
247.194855892591,247.286653225675,247.374897347581,247.463128033518,247.551366652242,
247.63963457309,247.728002873732,247.816430684893,247.904988820996,247.929234557263,
248.017786709342,248.106224104865,248.194570548063,248.286367881147,248.374612003053,
248.462842688989,248.551081307713,248.639349228561,248.727717529202,248.816145340363,
248.904703476466,248.928949212735,249.017501364815,249.105938760338,249.194285203536,
249.28608253662,249.374326658526,249.462557344462,249.550795963186,249.639063884034,
249.727432184675,249.815859995837,249.904418131939,249.928663868208,250.017216020288,
250.105653415811,250.193999859009,250.285797192093,250.374041313999,250.462271999935,
250.550510618659,250.638778539508,250.727146840149,250.81557465131,250.904132787413,
250.928378523681,251.016930675761,251.105368071284,251.193714514482,251.285511847566,
251.373755969472,251.461986655409,251.550225274133,251.63849319498,251.726861495621,
251.815289306782,251.903847442885,251.928093179154,252.020823214331,252.113389862077,
252.205749459193,252.297985132798,252.390068284817,252.437457498096),
 .UNSPECIFIED.);
#350=B_SPLINE_CURVE_WITH_KNOTS('',3,(#57807,#57808,#57809,#57810,#57811,
#57812,#57813,#57814,#57815,#57816,#57817,#57818,#57819,#57820,#57821,#57822,
#57823,#57824,#57825,#57826,#57827,#57828,#57829,#57830,#57831,#57832,#57833,
#57834,#57835,#57836,#57837,#57838,#57839,#57840,#57841,#57842,#57843,#57844,
#57845,#57846,#57847,#57848,#57849,#57850,#57851,#57852,#57853,#57854,#57855,
#57856,#57857,#57858,#57859,#57860,#57861,#57862,#57863,#57864,#57865,#57866,
#57867,#57868,#57869,#57870,#57871,#57872,#57873,#57874,#57875,#57876,#57877,
#57878,#57879,#57880,#57881,#57882,#57883,#57884,#57885,#57886,#57887,#57888,
#57889,#57890,#57891,#57892,#57893,#57894,#57895,#57896,#57897,#57898,#57899,
#57900,#57901,#57902,#57903,#57904,#57905,#57906,#57907,#57908,#57909,#57910,
#57911,#57912,#57913,#57914,#57915,#57916,#57917,#57918,#57919,#57920,#57921,
#57922,#57923,#57924,#57925,#57926,#57927,#57928,#57929,#57930,#57931,#57932,
#57933,#57934,#57935,#57936,#57937,#57938,#57939,#57940,#57941,#57942,#57943,
#57944,#57945,#57946,#57947,#57948,#57949,#57950,#57951,#57952,#57953,#57954,
#57955,#57956,#57957,#57958,#57959,#57960,#57961,#57962,#57963,#57964,#57965,
#57966,#57967,#57968,#57969,#57970,#57971,#57972,#57973,#57974,#57975,#57976,
#57977,#57978,#57979,#57980,#57981,#57982,#57983,#57984,#57985,#57986,#57987,
#57988,#57989,#57990,#57991,#57992,#57993,#57994,#57995,#57996,#57997,#57998,
#57999,#58000,#58001,#58002,#58003,#58004,#58005,#58006,#58007,#58008,#58009,
#58010,#58011,#58012,#58013,#58014,#58015,#58016,#58017,#58018,#58019,#58020,
#58021,#58022,#58023,#58024,#58025,#58026,#58027,#58028,#58029,#58030,#58031,
#58032),.UNSPECIFIED.,.F.,.F.,(4,3,3,3,3,3,3,3,3,3,3,3,3,3,3,3,3,3,3,3,
3,3,3,3,3,3,3,3,3,3,3,3,3,3,3,3,3,3,3,3,3,3,3,3,3,3,3,3,3,3,3,3,3,3,3,3,
3,3,3,3,3,3,3,3,3,3,3,3,3,3,3,3,3,3,3,4),(252.437457498304,252.530258428474,
252.623203058074,252.716386016105,252.809701689193,252.903229080169,252.927807834627,
253.016359986706,253.104797382229,253.193143825426,253.28494115851,253.373185280416,
253.461415966351,253.549654585075,253.637922505923,253.726290806563,253.814718617724,
253.903276753826,253.927522490099,254.016074642179,254.104512037702,254.1928584809,
254.284655813984,254.37289993589,254.461130621826,254.54936924055,254.637637161398,
254.72600546204,254.814433273201,254.902991409303,254.927237145572,255.015789297652,
255.104226693175,255.192573136374,255.284370469458,255.372614591364,255.4608452773,
255.549083896024,255.637351816873,255.725720117514,255.814147928676,255.902706064779,
255.926951801045,256.015503953125,256.103941348648,256.192287791846,256.28408512493,
256.372329246836,256.460559932772,256.548798551496,256.637066472344,256.725434772985,
256.813862584146,256.902420720249,256.926666456518,257.015218608598,257.103656004121,
257.192002447319,257.283799780403,257.372043902309,257.460274588245,257.548513206969,
257.636781127818,257.725149428459,257.81357723962,257.902135375723,257.926381111991,
258.013674483031,258.102045523312,258.189121133445,258.276140912924,258.363127375888,
258.452506233235,258.539523844794,258.630083325035,258.720642805276),
 .UNSPECIFIED.);
#351=B_SPLINE_CURVE_WITH_KNOTS('',3,(#58034,#58035,#58036,#58037,#58038,
#58039,#58040,#58041,#58042,#58043,#58044),.UNSPECIFIED.,.F.,.F.,(4,1,1,
1,1,1,1,1,4),(258.720642805276,258.926095767464,259.925810422936,260.925525078409,
261.925239733882,262.924954389355,263.924669044828,264.924383700301,265.003828112455),
 .UNSPECIFIED.);
#352=B_SPLINE_CURVE_WITH_KNOTS('',3,(#58046,#58047,#58048,#58049,#58050,
#58051,#58052,#58053,#58054,#58055),.UNSPECIFIED.,.F.,.F.,(4,1,1,1,1,1,
1,4),(265.003828112455,265.924098355773,266.923813011246,267.923527666719,
268.923242322192,269.922956977665,270.922671633138,271.287013419635),
 .UNSPECIFIED.);
#353=B_SPLINE_CURVE_WITH_KNOTS('',3,(#58057,#58058,#58059,#58060,#58061,
#58062,#58063,#58064,#58065,#58066),.UNSPECIFIED.,.F.,.F.,(4,1,1,1,1,1,
1,4),(271.287013419635,271.92238628861,272.922100944083,273.921815599556,
274.921530255029,275.921244910502,276.920959565975,277.570198726814),
 .UNSPECIFIED.);
#354=B_SPLINE_CURVE_WITH_KNOTS('',3,(#58068,#58069,#58070,#58071,#58072,
#58073,#58074,#58075,#58076,#58077,#58078,#58079,#58080,#58081,#58082,#58083,
#58084,#58085,#58086,#58087,#58088,#58089,#58090,#58091,#58092,#58093,#58094,
#58095,#58096,#58097,#58098,#58099,#58100,#58101,#58102,#58103,#58104,#58105,
#58106,#58107,#58108,#58109,#58110,#58111,#58112,#58113,#58114,#58115,#58116,
#58117,#58118,#58119,#58120,#58121,#58122,#58123,#58124,#58125,#58126,#58127,
#58128,#58129,#58130,#58131,#58132,#58133,#58134,#58135,#58136,#58137,#58138,
#58139,#58140,#58141,#58142,#58143,#58144,#58145,#58146,#58147,#58148,#58149,
#58150,#58151,#58152,#58153,#58154,#58155,#58156,#58157,#58158,#58159,#58160,
#58161,#58162,#58163,#58164,#58165,#58166,#58167,#58168,#58169,#58170,#58171,
#58172,#58173,#58174,#58175,#58176,#58177,#58178,#58179,#58180,#58181,#58182,
#58183,#58184,#58185,#58186,#58187,#58188,#58189,#58190,#58191,#58192,#58193,
#58194,#58195,#58196,#58197,#58198,#58199,#58200,#58201,#58202,#58203,#58204,
#58205,#58206,#58207,#58208,#58209,#58210,#58211,#58212,#58213,#58214,#58215,
#58216,#58217,#58218,#58219,#58220,#58221,#58222,#58223,#58224,#58225,#58226,
#58227,#58228,#58229,#58230,#58231,#58232,#58233,#58234,#58235,#58236,#58237,
#58238,#58239,#58240,#58241,#58242,#58243,#58244,#58245,#58246,#58247,#58248,
#58249,#58250,#58251,#58252,#58253,#58254,#58255,#58256,#58257,#58258,#58259,
#58260,#58261,#58262,#58263,#58264,#58265,#58266,#58267,#58268,#58269,#58270,
#58271,#58272,#58273,#58274,#58275,#58276,#58277,#58278,#58279,#58280,#58281,
#58282,#58283,#58284,#58285,#58286,#58287,#58288,#58289,#58290,#58291,#58292,
#58293),.UNSPECIFIED.,.F.,.F.,(4,3,3,3,3,3,3,3,3,3,3,3,3,3,3,3,3,3,3,3,
3,3,3,3,3,3,3,3,3,3,3,3,3,3,3,3,3,3,3,3,3,3,3,3,3,3,3,3,3,3,3,3,3,3,3,3,
3,3,3,3,3,3,3,3,3,3,3,3,3,3,3,3,3,3,3,4),(277.570198972254,277.671486989444,
277.773303087998,277.875759025028,277.920674221447,278.009226373527,278.09766376905,
278.186010212248,278.277807545332,278.366051667238,278.454282353174,278.542520971898,
278.630788892746,278.719157193388,278.807585004549,278.896143140652,278.92038887692,
279.008941029,279.097378424523,279.185724867721,279.277522200805,279.365766322711,
279.453997008647,279.542235627371,279.630503548219,279.718871848861,279.807299660022,
279.895857796125,279.920103532393,280.008655684473,280.097093079996,280.185439523194,
280.277236856278,280.365480978184,280.45371166412,280.541950282844,280.630218203692,
280.718586504333,280.807014315494,280.895572451597,280.919818187866,281.008370339946,
281.096807735469,281.185154178667,281.276951511751,281.365195633657,281.453426319593,
281.541664938317,281.629932859166,281.718301159807,281.806728970968,281.895287107071,
281.919532843339,282.008084995419,282.096522390942,282.18486883414,282.276666167224,
282.36491028913,282.453140975067,282.54137959379,282.629647514639,282.71801581528,
282.806443626441,282.895001762544,282.919247498812,283.006962242243,283.094562935591,
283.182074273176,283.269522395889,283.356937750207,283.444342502134,283.531758804621,
283.619259545184,283.706805501756,283.794483384449,283.853384033994),
 .UNSPECIFIED.);
#355=B_SPLINE_CURVE_WITH_KNOTS('',3,(#58295,#58296,#58297,#58298,#58299,
#58300,#58301,#58302,#58303,#58304,#58305,#58306),.UNSPECIFIED.,.F.,.F.,
(4,2,1,1,1,1,1,1,4),(283.853384033994,283.918962154284,284.918676809757,
285.91839146523,286.918106120703,287.917820776176,288.917535431649,289.917250087121,
290.136569341174),.UNSPECIFIED.);
#356=B_SPLINE_CURVE_WITH_KNOTS('',3,(#58308,#58309,#58310,#58311,#58312,
#58313,#58314,#58315,#58316,#58317,#58318,#58319,#58320,#58321,#58322,#58323,
#58324,#58325,#58326,#58327,#58328,#58329,#58330,#58331,#58332,#58333,#58334,
#58335,#58336,#58337,#58338,#58339,#58340,#58341,#58342,#58343,#58344,#58345,
#58346,#58347,#58348,#58349,#58350,#58351,#58352,#58353,#58354,#58355,#58356,
#58357,#58358,#58359,#58360,#58361,#58362,#58363,#58364,#58365,#58366,#58367,
#58368,#58369,#58370,#58371,#58372,#58373,#58374,#58375,#58376,#58377,#58378,
#58379,#58380,#58381,#58382,#58383,#58384,#58385,#58386,#58387,#58388,#58389,
#58390,#58391,#58392,#58393,#58394,#58395,#58396,#58397,#58398,#58399,#58400,
#58401,#58402,#58403,#58404,#58405,#58406,#58407,#58408,#58409,#58410,#58411,
#58412,#58413,#58414,#58415,#58416,#58417,#58418,#58419,#58420,#58421,#58422,
#58423,#58424,#58425,#58426,#58427,#58428,#58429,#58430,#58431,#58432,#58433,
#58434,#58435,#58436,#58437,#58438,#58439,#58440,#58441,#58442,#58443,#58444,
#58445,#58446,#58447,#58448,#58449,#58450,#58451,#58452,#58453,#58454,#58455,
#58456,#58457,#58458,#58459,#58460,#58461,#58462,#58463,#58464,#58465,#58466,
#58467,#58468,#58469,#58470,#58471,#58472,#58473,#58474,#58475,#58476,#58477,
#58478,#58479,#58480,#58481,#58482,#58483,#58484,#58485,#58486,#58487,#58488,
#58489,#58490,#58491,#58492,#58493,#58494,#58495,#58496,#58497,#58498,#58499,
#58500,#58501,#58502,#58503,#58504,#58505,#58506,#58507,#58508,#58509,#58510,
#58511,#58512,#58513,#58514,#58515,#58516,#58517,#58518,#58519,#58520,#58521,
#58522,#58523,#58524,#58525,#58526,#58527,#58528,#58529,#58530,#58531,#58532,
#58533),.UNSPECIFIED.,.F.,.F.,(4,3,3,3,3,3,3,3,3,3,3,3,3,3,3,3,3,3,3,3,
3,3,3,3,3,3,3,3,3,3,3,3,3,3,3,3,3,3,3,3,3,3,3,3,3,3,3,3,3,3,3,3,3,3,3,3,
3,3,3,3,3,3,3,3,3,3,3,3,3,3,3,3,3,3,3,4),(290.136569341174,290.223730192393,
290.310821510838,290.397875760146,290.484915386051,290.571962817726,290.659095926046,
290.746271223774,290.833590646189,290.916964742594,291.005516894674,291.093954290197,
291.182300733395,291.274098066479,291.362342188385,291.450572874322,291.538811493046,
291.627079413894,291.715447714535,291.803875525696,291.892433661799,291.916679398067,
292.005231550147,292.09366894567,292.182015388868,292.273812721952,292.362056843858,
292.450287529794,292.538526148518,292.626794069366,292.715162370007,292.803590181168,
292.892148317271,292.91639405354,293.00494620562,293.093383601143,293.181730044341,
293.273527377425,293.361771499331,293.450002185267,293.538240803991,293.626508724839,
293.714877025481,293.803304836642,293.891862972745,293.916108709013,294.004660861093,
294.093098256616,294.181444699814,294.273242032898,294.361486154804,294.44971684074,
294.537955459464,294.626223380313,294.714591680955,294.803019492116,294.891577628219,
294.915823364486,295.004375516565,295.092812912088,295.181159355286,295.27295668837,
295.361200810276,295.449431496212,295.537670114935,295.625938035784,295.714306336425,
295.802734147586,295.891292283689,295.915538019958,296.008475344092,296.10124593225,
296.193803345762,296.286232444007,296.378502206548,296.419754648353),
 .UNSPECIFIED.);
#357=B_SPLINE_CURVE_WITH_KNOTS('',3,(#58535,#58536,#58537,#58538,#58539,
#58540,#58541,#58542,#58543,#58544,#58545,#58546,#58547,#58548,#58549,#58550,
#58551,#58552,#58553,#58554,#58555,#58556,#58557,#58558,#58559,#58560,#58561,
#58562,#58563,#58564,#58565,#58566,#58567,#58568,#58569,#58570,#58571,#58572,
#58573,#58574,#58575,#58576,#58577,#58578,#58579,#58580,#58581,#58582,#58583,
#58584,#58585,#58586,#58587,#58588,#58589,#58590,#58591,#58592,#58593,#58594,
#58595,#58596,#58597,#58598,#58599,#58600,#58601,#58602,#58603,#58604,#58605,
#58606,#58607,#58608,#58609,#58610,#58611,#58612,#58613,#58614,#58615,#58616,
#58617,#58618,#58619,#58620,#58621,#58622,#58623,#58624,#58625,#58626,#58627,
#58628,#58629,#58630,#58631,#58632,#58633,#58634,#58635,#58636,#58637,#58638,
#58639,#58640,#58641,#58642,#58643,#58644,#58645,#58646,#58647,#58648,#58649,
#58650,#58651,#58652,#58653,#58654,#58655,#58656,#58657,#58658,#58659,#58660,
#58661,#58662,#58663,#58664,#58665,#58666,#58667,#58668,#58669,#58670,#58671,
#58672,#58673,#58674,#58675,#58676,#58677,#58678,#58679,#58680,#58681,#58682,
#58683,#58684,#58685,#58686,#58687,#58688,#58689,#58690,#58691,#58692,#58693,
#58694,#58695,#58696,#58697,#58698,#58699,#58700,#58701,#58702,#58703,#58704,
#58705,#58706,#58707,#58708,#58709,#58710,#58711,#58712,#58713,#58714,#58715,
#58716,#58717,#58718,#58719,#58720,#58721,#58722,#58723,#58724,#58725,#58726,
#58727,#58728,#58729,#58730,#58731,#58732,#58733,#58734,#58735,#58736,#58737,
#58738,#58739,#58740,#58741,#58742,#58743,#58744,#58745,#58746,#58747,#58748,
#58749,#58750,#58751,#58752,#58753,#58754,#58755,#58756,#58757,#58758,#58759,
#58760),.UNSPECIFIED.,.F.,.F.,(4,3,3,3,3,3,3,3,3,3,3,3,3,3,3,3,3,3,3,3,
3,3,3,3,3,3,3,3,3,3,3,3,3,3,3,3,3,3,3,3,3,3,3,3,3,3,3,3,3,3,3,3,3,3,3,3,
3,3,3,3,3,3,3,3,3,3,3,3,3,3,3,3,3,3,3,4),(296.419754648543,296.512351451628,
296.605083805464,296.698046710968,296.79113719593,296.884437934939,296.915252675431,
297.003804827511,297.092242223034,297.180588666232,297.272385999316,297.360630121222,
297.448860807159,297.537099425883,297.625367346731,297.713735647373,297.802163458534,
297.890721594637,297.914967330904,298.003519482984,298.091956878507,298.180303321705,
298.272100654789,298.360344776695,298.448575462631,298.536814081355,298.625082002203,
298.713450302845,298.801878114006,298.890436250109,298.914681986377,299.003234138457,
299.09167153398,299.180017977178,299.271815310262,299.360059432168,299.448290118104,
299.536528736828,299.624796657676,299.713164958317,299.801592769478,299.890150905581,
299.91439664185,300.00294879393,300.091386189453,300.179732632651,300.271529965735,
300.359774087641,300.448004773578,300.536243392302,300.62451131315,300.712879613792,
300.801307424953,300.889865561056,300.914111297323,301.002663449402,301.091100844925,
301.179447288123,301.271244621207,301.359488743113,301.447719429049,301.535958047772,
301.624225968621,301.712594269262,301.801022080423,301.889580216525,301.913825952795,
302.001138292507,302.088863500385,302.17595801984,302.262996307226,302.350000864675,
302.43823563739,302.525269190206,302.61410457287,302.702939955533),
 .UNSPECIFIED.);
#358=B_SPLINE_CURVE_WITH_KNOTS('',3,(#58762,#58763,#58764,#58765,#58766,
#58767,#58768,#58769,#58770,#58771,#58772),.UNSPECIFIED.,.F.,.F.,(4,1,1,
1,1,1,1,1,4),(302.702939955533,302.913540608268,303.913255263741,304.912969919214,
305.912684574687,306.91239923016,307.912113885632,308.911828541105,308.986125262712),
 .UNSPECIFIED.);
#359=B_SPLINE_CURVE_WITH_KNOTS('',3,(#58774,#58775,#58776,#58777,#58778,
#58779,#58780,#58781,#58782,#58783),.UNSPECIFIED.,.F.,.F.,(4,1,1,1,1,1,
1,4),(308.986125262712,309.911543196578,310.911257852051,311.910972507524,
312.910687162997,313.910401818469,314.910116473942,315.269310569892),
 .UNSPECIFIED.);
#360=B_SPLINE_CURVE_WITH_KNOTS('',3,(#58785,#58786,#58787,#58788,#58789,
#58790,#58791,#58792,#58793,#58794),.UNSPECIFIED.,.F.,.F.,(4,1,1,1,1,1,
1,4),(315.269310569892,315.909831129415,316.909545784888,317.909260440361,
318.908975095834,319.908689751306,320.908404406779,321.552495877071),
 .UNSPECIFIED.);
#361=B_SPLINE_CURVE_WITH_KNOTS('',3,(#58796,#58797,#58798,#58799,#58800,
#58801,#58802,#58803,#58804,#58805,#58806,#58807,#58808,#58809,#58810,#58811,
#58812,#58813,#58814,#58815,#58816,#58817,#58818,#58819,#58820,#58821,#58822,
#58823,#58824,#58825,#58826,#58827,#58828,#58829,#58830,#58831,#58832,#58833,
#58834,#58835,#58836,#58837,#58838,#58839,#58840,#58841,#58842,#58843,#58844,
#58845,#58846,#58847,#58848,#58849,#58850,#58851,#58852,#58853,#58854,#58855,
#58856,#58857,#58858,#58859,#58860,#58861,#58862,#58863,#58864,#58865,#58866,
#58867,#58868,#58869,#58870,#58871,#58872,#58873,#58874,#58875,#58876,#58877,
#58878,#58879,#58880,#58881,#58882,#58883,#58884,#58885,#58886,#58887,#58888,
#58889,#58890,#58891,#58892,#58893,#58894,#58895,#58896,#58897,#58898,#58899,
#58900,#58901,#58902,#58903,#58904,#58905,#58906,#58907,#58908,#58909,#58910,
#58911,#58912,#58913,#58914,#58915,#58916,#58917,#58918,#58919,#58920,#58921,
#58922,#58923,#58924,#58925,#58926,#58927,#58928,#58929,#58930,#58931,#58932,
#58933,#58934,#58935,#58936,#58937,#58938,#58939,#58940,#58941,#58942,#58943,
#58944,#58945,#58946,#58947,#58948,#58949,#58950,#58951,#58952,#58953,#58954,
#58955,#58956,#58957,#58958,#58959,#58960,#58961,#58962,#58963,#58964,#58965,
#58966,#58967,#58968,#58969,#58970,#58971,#58972,#58973,#58974,#58975,#58976,
#58977,#58978,#58979,#58980,#58981,#58982,#58983,#58984,#58985,#58986,#58987,
#58988,#58989,#58990,#58991,#58992,#58993,#58994,#58995,#58996,#58997,#58998,
#58999,#59000,#59001,#59002,#59003,#59004,#59005,#59006,#59007,#59008,#59009,
#59010,#59011,#59012,#59013,#59014,#59015,#59016,#59017,#59018,#59019,#59020,
#59021),.UNSPECIFIED.,.F.,.F.,(4,3,3,3,3,3,3,3,3,3,3,3,3,3,3,3,3,3,3,3,
3,3,3,3,3,3,3,3,3,3,3,3,3,3,3,3,3,3,3,3,3,3,3,3,3,3,3,3,3,3,3,3,3,3,3,3,
3,3,3,3,3,3,3,3,3,3,3,3,3,3,3,3,3,3,3,4),(321.55249612466,321.653352335466,
321.754706689964,321.856679710689,321.908119062252,321.996671214331,322.085108609854,
322.173455053052,322.265252386136,322.353496508042,322.441727193978,322.529965812702,
322.61823373355,322.706602034191,322.795029845352,322.883587981454,322.907833717725,
322.996385869805,323.084823265328,323.173169708526,323.26496704161,323.353211163516,
323.441441849452,323.529680468176,323.617948389025,323.706316689666,323.794744500827,
323.88330263693,323.907548373198,323.996100525278,324.084537920801,324.172884363999,
324.264681697083,324.35292581899,324.441156504926,324.52939512365,324.617663044498,
324.70603134514,324.794459156301,324.883017292404,324.907263028671,324.99581518075,
325.084252576273,325.172599019471,325.264396352555,325.352640474461,325.440871160397,
325.529109779121,325.617377699969,325.70574600061,325.794173811771,325.882731947873,
325.906977684143,325.995529836223,326.083967231746,326.172313674944,326.264111008028,
326.352355129934,326.44058581587,326.528824434594,326.617092355442,326.705460656083,
326.793888467244,326.882446603347,326.906692339616,326.994359313025,327.081912284458,
327.169375991889,327.256776540059,327.344144456776,327.431501945575,327.518871197051,
327.606324201979,327.693822711221,327.781450815237,327.835681184251),
 .UNSPECIFIED.);
#362=B_SPLINE_CURVE_WITH_KNOTS('',3,(#59023,#59024,#59025,#59026,#59027,
#59028,#59029,#59030,#59031,#59032,#59033),.UNSPECIFIED.,.F.,.F.,(4,1,1,
1,1,1,1,1,4),(327.835681184251,327.906406995089,328.906121650562,329.905836306035,
330.905550961508,331.90526561698,332.904980272453,333.904694927926,334.118866491431),
 .UNSPECIFIED.);
#363=B_SPLINE_CURVE_WITH_KNOTS('',3,(#59035,#59036,#59037,#59038,#59039,
#59040,#59041,#59042,#59043,#59044),.UNSPECIFIED.,.F.,.F.,(4,1,1,1,1,1,
1,4),(334.118866491431,334.904409583399,335.904124238872,336.903838894345,
337.903553549817,338.90326820529,339.902982860763,340.40205179861),
 .UNSPECIFIED.);
#364=B_SPLINE_CURVE_WITH_KNOTS('',3,(#59046,#59047,#59048,#59049,#59050,
#59051,#59052,#59053,#59054,#59055),.UNSPECIFIED.,.F.,.F.,(4,1,1,1,1,1,
1,4),(340.40205179861,340.902697516236,341.902412171709,342.902126827182,
343.901841482655,344.901556138127,345.9012707936,346.68523710579),
 .UNSPECIFIED.);
#365=B_SPLINE_CURVE_WITH_KNOTS('',3,(#59057,#59058,#59059,#59060,#59061,
#59062,#59063,#59064,#59065,#59066,#59067),.UNSPECIFIED.,.F.,.F.,(4,1,1,
1,1,1,1,1,4),(346.68523710579,346.900985449073,347.900700104546,348.900414760019,
349.900129415491,350.899844070964,351.899558726437,352.89927338191,352.968422412969),
 .UNSPECIFIED.);
#366=B_SPLINE_CURVE_WITH_KNOTS('',3,(#59069,#59070,#59071,#59072,#59073,
#59074,#59075,#59076,#59077,#59078,#59079,#59080,#59081,#59082,#59083,#59084,
#59085,#59086,#59087,#59088,#59089,#59090,#59091,#59092,#59093,#59094,#59095,
#59096,#59097,#59098,#59099,#59100,#59101,#59102,#59103,#59104,#59105,#59106,
#59107,#59108,#59109,#59110,#59111,#59112,#59113,#59114,#59115,#59116,#59117,
#59118,#59119,#59120,#59121,#59122,#59123,#59124,#59125,#59126,#59127,#59128,
#59129,#59130,#59131,#59132,#59133,#59134,#59135,#59136,#59137,#59138,#59139,
#59140,#59141,#59142,#59143,#59144,#59145,#59146,#59147,#59148,#59149,#59150,
#59151,#59152,#59153,#59154,#59155,#59156,#59157,#59158,#59159,#59160,#59161,
#59162,#59163,#59164,#59165,#59166,#59167,#59168,#59169,#59170,#59171,#59172,
#59173,#59174,#59175,#59176,#59177,#59178,#59179,#59180,#59181,#59182,#59183,
#59184,#59185,#59186,#59187,#59188,#59189,#59190,#59191,#59192,#59193,#59194,
#59195,#59196,#59197,#59198,#59199,#59200,#59201,#59202,#59203,#59204,#59205,
#59206,#59207,#59208,#59209,#59210,#59211,#59212,#59213,#59214,#59215,#59216,
#59217,#59218,#59219,#59220,#59221,#59222,#59223,#59224,#59225,#59226,#59227,
#59228,#59229,#59230,#59231,#59232,#59233,#59234,#59235,#59236,#59237,#59238,
#59239,#59240,#59241,#59242,#59243,#59244,#59245,#59246,#59247,#59248,#59249,
#59250,#59251,#59252,#59253,#59254,#59255,#59256,#59257,#59258,#59259,#59260,
#59261,#59262,#59263,#59264,#59265,#59266,#59267,#59268,#59269,#59270,#59271,
#59272,#59273,#59274,#59275,#59276,#59277,#59278,#59279,#59280,#59281,#59282,
#59283,#59284,#59285,#59286,#59287,#59288,#59289,#59290,#59291,#59292,#59293,
#59294),.UNSPECIFIED.,.F.,.F.,(4,3,3,3,3,3,3,3,3,3,3,3,3,3,3,3,3,3,3,3,
3,3,3,3,3,3,3,3,3,3,3,3,3,3,3,3,3,3,3,3,3,3,3,3,3,3,3,3,3,3,3,3,3,3,3,3,
3,3,3,3,3,3,3,3,3,3,3,3,3,3,3,3,3,3,3,4),(352.968422412969,353.056076536257,
353.143622164665,353.231083997544,353.318490920333,353.40587026875,353.493244230893,
353.580634986258,353.668117469944,353.755649754035,353.843319148401,353.898988037383,
353.987540189463,354.075977584986,354.164324028184,354.256121361268,354.344365483174,
354.43259616911,354.520834787834,354.609102708682,354.697471009324,354.785898820485,
354.874456956588,354.898702692856,354.987254844935,355.075692240458,355.164038683656,
355.25583601674,355.344080138646,355.432310824582,355.520549443305,355.608817364153,
355.697185664794,355.785613475955,355.874171612058,355.898417348328,355.986969500408,
356.075406895931,356.163753339129,356.255550672213,356.343794794119,356.432025480055,
356.520264098779,356.608532019628,356.696900320269,356.78532813143,356.873886267533,
356.898132003801,356.986684155881,357.075121551404,357.163467994602,357.255265327686,
357.343509449593,357.431740135529,357.519978754253,357.608246675101,357.696614975743,
357.785042786904,357.873600923007,357.897846659274,357.986398811353,358.074836206877,
358.163182650075,358.254979983159,358.343224105065,358.431454791001,358.519693409725,
358.607961330574,358.696329631215,358.784757442376,358.873315578479,358.897561314747,
358.999617211864,359.101261411547,359.202154318896,359.25160747295),
 .UNSPECIFIED.);
#367=B_SPLINE_CURVE_WITH_KNOTS('',3,(#59296,#59297,#59298,#59299,#59300,
#59301,#59302,#59303,#59304,#59305),.UNSPECIFIED.,.F.,.F.,(4,1,1,1,1,1,
1,4),(359.251607720149,359.89727597022,360.896990625693,361.896705281165,
362.896419936638,363.896134592111,364.895849247584,365.534793027328),
 .UNSPECIFIED.);
#368=B_SPLINE_CURVE_WITH_KNOTS('',3,(#59307,#59308,#59309,#59310,#59311,
#59312,#59313,#59314,#59315,#59316),.UNSPECIFIED.,.F.,.F.,(4,1,1,1,1,1,
1,4),(365.534793027328,365.895563903057,366.89527855853,367.894993214002,
368.894707869475,369.894422524948,370.894137180421,371.817978334508),
 .UNSPECIFIED.);
#369=B_SPLINE_CURVE_WITH_KNOTS('',3,(#59318,#59319,#59320,#59321,#59322,
#59323,#59324,#59325,#59326,#59327,#59328),.UNSPECIFIED.,.F.,.F.,(4,1,1,
1,1,1,1,1,4),(371.817978334508,371.893851835894,372.893566491367,373.893281146839,
374.892995802312,375.892710457785,376.892425113258,377.892139768731,378.101163641688),
 .UNSPECIFIED.);
#370=B_SPLINE_CURVE_WITH_KNOTS('',3,(#59330,#59331,#59332,#59333,#59334,
#59335,#59336,#59337,#59338,#59339,#59340,#59341,#59342,#59343,#59344,#59345,
#59346,#59347,#59348,#59349,#59350,#59351,#59352,#59353,#59354,#59355,#59356,
#59357,#59358,#59359,#59360,#59361,#59362,#59363,#59364,#59365,#59366,#59367,
#59368,#59369,#59370,#59371,#59372,#59373,#59374,#59375,#59376,#59377,#59378,
#59379,#59380,#59381,#59382,#59383,#59384,#59385,#59386,#59387,#59388,#59389,
#59390,#59391,#59392,#59393,#59394,#59395,#59396,#59397,#59398,#59399,#59400,
#59401,#59402,#59403,#59404,#59405,#59406,#59407,#59408,#59409,#59410,#59411,
#59412,#59413,#59414,#59415,#59416,#59417,#59418,#59419,#59420,#59421,#59422,
#59423,#59424,#59425,#59426,#59427,#59428,#59429,#59430,#59431,#59432,#59433,
#59434,#59435,#59436,#59437,#59438,#59439,#59440,#59441,#59442,#59443,#59444,
#59445,#59446,#59447,#59448,#59449,#59450,#59451,#59452,#59453,#59454,#59455,
#59456,#59457,#59458,#59459,#59460,#59461,#59462,#59463,#59464,#59465,#59466,
#59467,#59468,#59469,#59470,#59471,#59472,#59473,#59474,#59475,#59476,#59477,
#59478,#59479,#59480,#59481,#59482,#59483,#59484,#59485,#59486,#59487,#59488,
#59489,#59490,#59491,#59492,#59493,#59494,#59495,#59496,#59497,#59498,#59499,
#59500,#59501,#59502,#59503,#59504,#59505,#59506,#59507,#59508,#59509,#59510,
#59511,#59512,#59513,#59514,#59515,#59516,#59517,#59518,#59519,#59520,#59521,
#59522,#59523,#59524,#59525,#59526,#59527,#59528,#59529,#59530,#59531,#59532,
#59533,#59534,#59535,#59536,#59537,#59538,#59539,#59540,#59541,#59542,#59543,
#59544,#59545,#59546,#59547,#59548,#59549,#59550,#59551,#59552,#59553,#59554,
#59555),.UNSPECIFIED.,.F.,.F.,(4,3,3,3,3,3,3,3,3,3,3,3,3,3,3,3,3,3,3,3,
3,3,3,3,3,3,3,3,3,3,3,3,3,3,3,3,3,3,3,3,3,3,3,3,3,3,3,3,3,3,3,3,3,3,3,3,
3,3,3,3,3,3,3,3,3,3,3,3,3,3,3,3,3,3,3,4),(378.101163641688,378.188294434811,
378.276239433485,378.363255340551,378.45025374502,378.53725710691,378.625906436233,
378.71303415997,378.802444292087,378.891854424203,378.980406576283,379.068843971806,
379.157190415004,379.248987748088,379.337231869994,379.425462555931,379.513701174655,
379.601969095503,379.690337396145,379.778765207306,379.867323343409,379.891569079676,
379.980121231756,380.068558627279,380.156905070477,380.248702403561,380.336946525467,
380.425177211403,380.513415830127,380.601683750975,380.690052051617,380.778479862778,
380.867037998881,380.891283735149,380.979835887229,381.068273282752,381.15661972595,
381.248417059034,381.33666118094,381.424891866876,381.5131304856,381.601398406448,
381.68976670709,381.778194518251,381.866752654354,381.890998390622,381.979550542702,
382.067987938225,382.156334381423,382.248131714507,382.336375836413,382.424606522349,
382.512845141073,382.601113061921,382.689481362562,382.777909173723,382.866467309826,
382.890713046095,382.979265198175,383.067702593698,383.156049036896,383.24784636998,
383.336090491886,383.424321177823,383.512559796546,383.600827717395,383.689196018036,
383.777623829197,383.8661819653,383.890427701568,383.983796145665,384.076990602884,
384.169958800033,384.262789039653,384.355445853662,384.384348948737),
 .UNSPECIFIED.);
#371=B_SPLINE_CURVE_WITH_KNOTS('',3,(#59557,#59558,#59559,#59560,#59561,
#59562,#59563,#59564,#59565,#59566,#59567,#59568,#59569,#59570,#59571,#59572,
#59573,#59574,#59575,#59576,#59577,#59578,#59579,#59580,#59581,#59582,#59583,
#59584,#59585,#59586,#59587,#59588,#59589,#59590,#59591,#59592,#59593,#59594,
#59595,#59596,#59597,#59598,#59599,#59600,#59601,#59602,#59603,#59604,#59605,
#59606,#59607,#59608,#59609,#59610,#59611,#59612,#59613,#59614,#59615,#59616,
#59617,#59618,#59619,#59620,#59621,#59622,#59623,#59624,#59625,#59626,#59627,
#59628,#59629,#59630,#59631,#59632,#59633,#59634,#59635,#59636,#59637,#59638,
#59639,#59640,#59641,#59642,#59643,#59644,#59645,#59646,#59647,#59648,#59649,
#59650,#59651,#59652,#59653,#59654,#59655,#59656,#59657,#59658,#59659,#59660,
#59661,#59662,#59663,#59664,#59665,#59666,#59667,#59668,#59669,#59670,#59671,
#59672,#59673,#59674,#59675,#59676,#59677,#59678,#59679,#59680,#59681,#59682,
#59683,#59684,#59685,#59686,#59687,#59688,#59689,#59690,#59691,#59692,#59693,
#59694,#59695,#59696,#59697,#59698,#59699,#59700,#59701,#59702,#59703,#59704,
#59705,#59706,#59707,#59708,#59709,#59710,#59711,#59712,#59713,#59714,#59715,
#59716,#59717,#59718,#59719,#59720,#59721,#59722,#59723,#59724,#59725,#59726,
#59727,#59728,#59729,#59730,#59731,#59732,#59733,#59734,#59735,#59736,#59737,
#59738,#59739,#59740,#59741,#59742,#59743,#59744,#59745,#59746,#59747,#59748,
#59749,#59750,#59751,#59752,#59753,#59754,#59755,#59756,#59757,#59758,#59759,
#59760,#59761,#59762,#59763,#59764,#59765,#59766,#59767,#59768,#59769,#59770,
#59771,#59772,#59773,#59774,#59775,#59776,#59777,#59778,#59779,#59780,#59781,
#59782),.UNSPECIFIED.,.F.,.F.,(4,3,3,3,3,3,3,3,3,3,3,3,3,3,3,3,3,3,3,3,
3,3,3,3,3,3,3,3,3,3,3,3,3,3,3,3,3,3,3,3,3,3,3,3,3,3,3,3,3,3,3,3,3,3,3,3,
3,3,3,3,3,3,3,3,3,3,3,3,3,3,3,3,3,3,3,4),(384.384348948867,384.476552719823,
384.568876792834,384.661416748294,384.754074511718,384.846939805279,384.890142357041,
384.97869450912,385.067131904643,385.15547834784,385.247275680924,385.33551980283,
385.423750488766,385.511989107489,385.600257028336,385.688625328977,385.777053140138,
385.86561127624,385.889857012513,385.978409164593,386.066846560116,386.155193003314,
386.246990336398,386.335234458304,386.42346514424,386.511703762964,386.599971683812,
386.688339984454,386.776767795615,386.865325931717,386.889571667986,386.978123820066,
387.066561215589,387.154907658787,387.246704991871,387.334949113777,387.423179799714,
387.511418418438,387.599686339287,387.688054639928,387.776482451089,387.865040587192,
387.889286323459,387.977838475538,388.066275871061,388.15462231426,388.246419647344,
388.33466376925,388.422894455186,388.511133073909,388.599400994758,388.687769295399,
388.776197106561,388.864755242663,388.889000978932,388.977553131012,389.065990526535,
389.154336969733,389.246134302817,389.334378424723,389.422609110659,389.510847729383,
389.599115650232,389.687483950873,389.775911762034,389.864469898137,389.888715634405,
389.976073385051,390.063291913215,390.150431025801,390.237513252655,390.324561065973,
390.411628077518,390.498701051175,390.585857212418,390.667534256047),
 .UNSPECIFIED.);
#372=B_SPLINE_CURVE_WITH_KNOTS('',3,(#59784,#59785,#59786,#59787,#59788,
#59789,#59790,#59791,#59792,#59793,#59794),.UNSPECIFIED.,.F.,.F.,(4,1,1,
1,1,1,1,1,4),(390.667534256047,390.888430289877,391.88814494535,392.887859600823,
393.887574256296,394.887288911769,395.887003567242,396.886718222715,396.950719563226),
 .UNSPECIFIED.);
#373=B_SPLINE_CURVE_WITH_KNOTS('',3,(#59796,#59797,#59798,#59799,#59800,
#59801,#59802,#59803,#59804,#59805,#59806,#59807,#59808,#59809,#59810,#59811,
#59812,#59813,#59814,#59815,#59816,#59817,#59818,#59819,#59820,#59821,#59822,
#59823,#59824,#59825,#59826,#59827,#59828,#59829,#59830,#59831,#59832,#59833,
#59834,#59835,#59836,#59837,#59838,#59839,#59840,#59841,#59842,#59843,#59844,
#59845,#59846,#59847,#59848,#59849,#59850,#59851,#59852,#59853,#59854,#59855,
#59856,#59857,#59858,#59859,#59860,#59861,#59862,#59863,#59864,#59865,#59866,
#59867,#59868,#59869,#59870,#59871,#59872,#59873,#59874,#59875,#59876,#59877,
#59878,#59879,#59880,#59881,#59882,#59883,#59884,#59885,#59886,#59887,#59888,
#59889,#59890,#59891,#59892,#59893,#59894,#59895,#59896,#59897,#59898,#59899,
#59900,#59901,#59902,#59903,#59904,#59905,#59906,#59907,#59908,#59909,#59910,
#59911,#59912,#59913,#59914,#59915,#59916,#59917,#59918,#59919,#59920,#59921,
#59922,#59923,#59924,#59925,#59926,#59927,#59928,#59929,#59930,#59931,#59932,
#59933,#59934,#59935,#59936,#59937,#59938,#59939,#59940,#59941,#59942,#59943,
#59944,#59945,#59946,#59947,#59948,#59949,#59950,#59951,#59952,#59953,#59954,
#59955,#59956,#59957,#59958,#59959,#59960,#59961,#59962,#59963,#59964,#59965,
#59966,#59967,#59968,#59969,#59970,#59971,#59972,#59973,#59974,#59975,#59976,
#59977,#59978,#59979,#59980,#59981,#59982,#59983,#59984,#59985,#59986,#59987,
#59988,#59989,#59990,#59991,#59992,#59993,#59994,#59995,#59996,#59997,#59998,
#59999,#60000,#60001,#60002,#60003,#60004,#60005,#60006,#60007,#60008,#60009,
#60010,#60011,#60012,#60013,#60014,#60015,#60016,#60017,#60018,#60019,#60020,
#60021),.UNSPECIFIED.,.F.,.F.,(4,3,3,3,3,3,3,3,3,3,3,3,3,3,3,3,3,3,3,3,
3,3,3,3,3,3,3,3,3,3,3,3,3,3,3,3,3,3,3,3,3,3,3,3,3,3,3,3,3,3,3,3,3,3,3,3,
3,3,3,3,3,3,3,3,3,3,3,3,3,3,3,3,3,3,3,4),(396.950719563226,397.038425769189,
397.12602269023,397.213534984691,397.300991215638,397.388419047536,397.475840630628,
397.563278105804,397.650806974123,397.738384760113,397.826101134347,397.886432878187,
397.974985030267,398.06342242579,398.151768868988,398.243566202072,398.331810323978,
398.420041009914,398.508279628638,398.596547549487,398.684915850128,398.773343661289,
398.861901797392,398.88614753366,398.97469968574,399.063137081263,399.151483524461,
399.243280857545,399.331524979451,399.419755665387,399.507994284112,399.59626220496,
399.684630505601,399.773058316762,399.861616452865,399.885862189133,399.974414341213,
400.062851736736,400.151198179933,400.242995513018,400.331239634924,400.41947032086,
400.507708939584,400.595976860432,400.684345161073,400.772772972234,400.861331108337,
400.885576844606,400.974128996686,401.062566392209,401.150912835407,401.242710168491,
401.330954290397,401.419184976333,401.507423595057,401.595691515906,401.684059816547,
401.772487627708,401.861045763811,401.885291500079,401.973843652159,402.062281047682,
402.15062749088,402.242424823964,402.33066894587,402.418899631806,402.50713825053,
402.595406171378,402.683774472019,402.77220228318,402.860760419283,402.885006155552,
402.987537932938,403.089635708668,403.190946113391,403.233904625629),
 .UNSPECIFIED.);
#374=B_SPLINE_CURVE_WITH_KNOTS('',3,(#60023,#60024,#60025,#60026,#60027,
#60028,#60029,#60030,#60031,#60032),.UNSPECIFIED.,.F.,.F.,(4,1,1,1,1,1,
1,4),(403.233904870406,403.884720811024,404.884435466497,405.88415012197,
406.883864777443,407.883579432916,408.883294088388,409.517090177585),
 .UNSPECIFIED.);
#375=B_SPLINE_CURVE_WITH_KNOTS('',3,(#60034,#60035,#60036,#60037,#60038,
#60039,#60040,#60041,#60042,#60043),.UNSPECIFIED.,.F.,.F.,(4,1,1,1,1,1,
1,4),(409.517090177585,409.883008743861,410.882723399334,411.882438054807,
412.88215271028,413.881867365753,414.881582021225,415.800275484765),
 .UNSPECIFIED.);
#376=B_SPLINE_CURVE_WITH_KNOTS('',3,(#60045,#60046,#60047,#60048,#60049,
#60050,#60051,#60052,#60053,#60054,#60055),.UNSPECIFIED.,.F.,.F.,(4,1,1,
1,1,1,1,1,4),(415.800275484765,415.881296676698,416.881011332171,417.880725987644,
418.880440643117,419.88015529859,420.879869954062,421.879584609535,422.083460791944),
 .UNSPECIFIED.);
#377=B_SPLINE_CURVE_WITH_KNOTS('',3,(#60057,#60058,#60059,#60060,#60061,
#60062,#60063,#60064,#60065,#60066,#60067,#60068,#60069,#60070,#60071,#60072,
#60073,#60074,#60075,#60076,#60077,#60078,#60079,#60080,#60081,#60082,#60083,
#60084,#60085,#60086,#60087,#60088,#60089,#60090,#60091,#60092,#60093,#60094,
#60095,#60096,#60097,#60098,#60099,#60100,#60101,#60102,#60103,#60104,#60105,
#60106,#60107,#60108,#60109,#60110,#60111,#60112,#60113,#60114,#60115,#60116,
#60117,#60118,#60119,#60120,#60121,#60122,#60123,#60124,#60125,#60126,#60127,
#60128,#60129,#60130,#60131,#60132,#60133,#60134,#60135,#60136,#60137,#60138,
#60139,#60140,#60141,#60142,#60143,#60144,#60145,#60146,#60147,#60148,#60149,
#60150,#60151,#60152,#60153,#60154,#60155,#60156,#60157,#60158,#60159,#60160,
#60161,#60162,#60163,#60164,#60165,#60166,#60167,#60168,#60169,#60170,#60171,
#60172,#60173,#60174,#60175,#60176,#60177,#60178,#60179,#60180,#60181,#60182,
#60183,#60184,#60185,#60186,#60187,#60188,#60189,#60190,#60191,#60192,#60193,
#60194,#60195,#60196,#60197,#60198,#60199,#60200,#60201,#60202,#60203,#60204,
#60205,#60206,#60207,#60208,#60209,#60210,#60211,#60212,#60213,#60214,#60215,
#60216,#60217,#60218,#60219,#60220,#60221,#60222,#60223,#60224,#60225,#60226,
#60227,#60228,#60229,#60230,#60231,#60232,#60233,#60234,#60235,#60236,#60237,
#60238,#60239,#60240,#60241,#60242,#60243,#60244,#60245,#60246,#60247,#60248,
#60249,#60250,#60251,#60252,#60253,#60254,#60255,#60256,#60257,#60258,#60259,
#60260,#60261,#60262,#60263,#60264,#60265,#60266,#60267,#60268,#60269,#60270,
#60271,#60272,#60273,#60274,#60275,#60276,#60277,#60278,#60279,#60280,#60281,
#60282),.UNSPECIFIED.,.F.,.F.,(4,3,3,3,3,3,3,3,3,3,3,3,3,3,3,3,3,3,3,3,
3,3,3,3,3,3,3,3,3,3,3,3,3,3,3,3,3,3,3,3,3,3,3,3,3,3,3,3,3,3,3,3,3,3,3,3,
3,3,3,3,3,3,3,3,3,3,3,3,3,3,3,3,3,3,3,4),(422.083460791944,422.170580161418,
422.259170049367,422.346170390656,422.433151884973,422.520137005079,422.609927570061,
422.697035626069,422.788167445539,422.879299265008,422.967851417088,423.056288812611,
423.144635255809,423.236432588893,423.324676710799,423.412907396735,423.501146015459,
423.589413936308,423.677782236949,423.76621004811,423.854768184213,423.879013920481,
423.967566072561,424.056003468084,424.144349911282,424.236147244366,424.324391366272,
424.412622052208,424.500860670932,424.58912859178,424.677496892421,424.765924703583,
424.854482839685,424.878728575954,424.967280728034,425.055718123557,425.144064566756,
425.235861899839,425.324106021746,425.412336707682,425.500575326406,425.588843247254,
425.677211547896,425.765639359057,425.85419749516,425.878443231427,425.966995383506,
426.055432779029,426.143779222227,426.235576555311,426.323820677217,426.412051363153,
426.500289981877,426.588557902725,426.676926203366,426.765354014527,426.853912150629,
426.878157886899,426.966710038978,427.055147434502,427.1434938777,427.235291210784,
427.32353533269,427.411766018626,427.500004637349,427.588272558198,427.67664085884,
427.765068670001,427.853626806103,427.877872542372,427.971465113027,428.064879770433,
428.158061167363,428.251099314232,428.34395673494,428.366646098882),
 .UNSPECIFIED.);
#378=B_SPLINE_CURVE_WITH_KNOTS('',3,(#60284,#60285,#60286,#60287,#60288,
#60289,#60290,#60291,#60292,#60293,#60294,#60295,#60296,#60297,#60298,#60299,
#60300,#60301,#60302,#60303,#60304,#60305,#60306,#60307,#60308,#60309,#60310,
#60311,#60312,#60313,#60314,#60315,#60316,#60317,#60318,#60319,#60320,#60321,
#60322,#60323,#60324,#60325,#60326,#60327,#60328,#60329,#60330,#60331,#60332,
#60333,#60334,#60335,#60336,#60337,#60338,#60339,#60340,#60341,#60342,#60343,
#60344,#60345,#60346,#60347,#60348,#60349,#60350,#60351,#60352,#60353,#60354,
#60355,#60356,#60357,#60358,#60359,#60360,#60361,#60362,#60363,#60364,#60365,
#60366,#60367,#60368,#60369,#60370,#60371,#60372,#60373,#60374,#60375,#60376,
#60377,#60378,#60379,#60380,#60381,#60382,#60383,#60384,#60385,#60386,#60387,
#60388,#60389,#60390,#60391,#60392,#60393,#60394,#60395,#60396,#60397,#60398,
#60399,#60400,#60401,#60402,#60403,#60404,#60405,#60406,#60407,#60408,#60409,
#60410,#60411,#60412,#60413,#60414,#60415,#60416,#60417,#60418,#60419,#60420,
#60421,#60422,#60423,#60424,#60425,#60426,#60427,#60428,#60429,#60430,#60431,
#60432,#60433,#60434,#60435,#60436,#60437,#60438,#60439,#60440,#60441,#60442,
#60443,#60444,#60445,#60446,#60447,#60448,#60449,#60450,#60451,#60452,#60453,
#60454,#60455,#60456,#60457,#60458,#60459,#60460,#60461,#60462,#60463,#60464,
#60465,#60466,#60467,#60468,#60469,#60470,#60471,#60472,#60473,#60474,#60475,
#60476,#60477,#60478,#60479,#60480,#60481,#60482,#60483,#60484,#60485,#60486,
#60487,#60488,#60489,#60490,#60491,#60492,#60493,#60494,#60495,#60496,#60497,
#60498,#60499,#60500,#60501,#60502,#60503,#60504,#60505,#60506,#60507,#60508,
#60509),.UNSPECIFIED.,.F.,.F.,(4,3,3,3,3,3,3,3,3,3,3,3,3,3,3,3,3,3,3,3,
3,3,3,3,3,3,3,3,3,3,3,3,3,3,3,3,3,3,3,3,3,3,3,3,3,3,3,3,3,3,3,3,3,3,3,3,
3,3,3,3,3,3,3,3,3,3,3,3,3,3,3,3,3,3,3,4),(428.366646099124,428.458660731681,
428.550788526121,428.643125281989,428.735575195126,428.828231383776,428.877587197845,
428.966139349925,429.054576745448,429.142923188646,429.23472052173,429.322964643636,
429.411195329572,429.499433948296,429.587701869144,429.676070169786,429.764497980947,
429.85305611705,429.877301853318,429.965854005398,430.054291400921,430.142637844119,
430.234435177203,430.322679299109,430.410909985045,430.499148603769,430.587416524617,
430.675784825259,430.76421263642,430.852770772523,430.877016508791,430.965568660871,
431.054006056394,431.142352499592,431.234149832676,431.322393954582,431.410624640519,
431.498863259243,431.587131180091,431.675499480732,431.763927291893,431.852485427996,
431.876731164264,431.965283316343,432.053720711866,432.142067155064,432.233864488148,
432.322108610054,432.41033929599,432.498577914713,432.586845835561,432.675214136202,
432.763641947363,432.852200083466,432.876445819736,432.964997971815,433.053435367338,
433.141781810536,433.23357914362,433.321823265527,433.410053951463,433.498292570186,
433.586560491034,433.674928791675,433.763356602836,433.851914738939,433.876160475209,
433.963544690523,434.050789271289,434.137954171459,434.225061902882,434.312134919759,
434.399225629821,434.486322069984,434.573498400505,434.649831406304),
 .UNSPECIFIED.);
#379=B_SPLINE_CURVE_WITH_KNOTS('',3,(#60511,#60512,#60513,#60514,#60515,
#60516,#60517,#60518,#60519,#60520,#60521),.UNSPECIFIED.,.F.,.F.,(4,1,1,
1,1,1,1,1,4),(434.649831406304,434.875875130682,435.875589786155,436.875304441628,
437.875019097101,438.874733752573,439.874448408046,440.874163063519,440.933016713483),
 .UNSPECIFIED.);
#380=B_SPLINE_CURVE_WITH_KNOTS('',3,(#60523,#60524,#60525,#60526,#60527,
#60528,#60529,#60530,#60531,#60532,#60533,#60534,#60535,#60536,#60537,#60538,
#60539,#60540,#60541,#60542,#60543,#60544,#60545,#60546,#60547,#60548,#60549,
#60550,#60551,#60552,#60553,#60554,#60555,#60556,#60557,#60558,#60559,#60560,
#60561,#60562,#60563,#60564,#60565,#60566,#60567,#60568,#60569,#60570,#60571,
#60572,#60573,#60574,#60575,#60576,#60577,#60578,#60579,#60580,#60581,#60582,
#60583,#60584,#60585,#60586,#60587,#60588,#60589,#60590,#60591,#60592,#60593,
#60594,#60595,#60596,#60597,#60598,#60599,#60600,#60601,#60602,#60603,#60604,
#60605,#60606,#60607,#60608,#60609,#60610,#60611,#60612,#60613,#60614,#60615,
#60616,#60617,#60618,#60619,#60620,#60621,#60622,#60623,#60624,#60625,#60626,
#60627,#60628,#60629,#60630,#60631,#60632,#60633,#60634,#60635,#60636,#60637,
#60638,#60639,#60640,#60641,#60642,#60643,#60644,#60645,#60646,#60647,#60648,
#60649,#60650,#60651,#60652,#60653,#60654,#60655,#60656,#60657,#60658,#60659,
#60660,#60661,#60662,#60663,#60664,#60665,#60666,#60667,#60668,#60669,#60670,
#60671,#60672,#60673,#60674,#60675,#60676,#60677,#60678,#60679,#60680,#60681,
#60682,#60683,#60684,#60685,#60686,#60687,#60688,#60689,#60690,#60691,#60692,
#60693,#60694,#60695,#60696,#60697,#60698,#60699,#60700,#60701,#60702,#60703,
#60704,#60705,#60706,#60707,#60708,#60709,#60710,#60711,#60712,#60713,#60714,
#60715,#60716,#60717,#60718,#60719,#60720,#60721,#60722,#60723,#60724,#60725,
#60726,#60727,#60728,#60729,#60730,#60731,#60732,#60733,#60734,#60735,#60736,
#60737,#60738,#60739,#60740,#60741,#60742,#60743,#60744,#60745,#60746,#60747,
#60748),.UNSPECIFIED.,.F.,.F.,(4,3,3,3,3,3,3,3,3,3,3,3,3,3,3,3,3,3,3,3,
3,3,3,3,3,3,3,3,3,3,3,3,3,3,3,3,3,3,3,3,3,3,3,3,3,3,3,3,3,3,3,3,3,3,3,3,
3,3,3,3,3,3,3,3,3,3,3,3,3,3,3,3,3,3,3,4),(440.933016713483,441.020777353221,
441.108427962358,441.195993154872,441.283501177297,441.370980007062,441.458451753743,
441.545938516856,441.633516355183,441.721142246195,441.808908214733,441.873877718992,
441.962429871072,442.050867266595,442.139213709793,442.231011042877,442.319255164783,
442.407485850719,442.495724469443,442.583992390291,442.672360690933,442.760788502094,
442.849346638197,442.873592374465,442.962144526545,443.050581922068,443.138928365266,
443.23072569835,443.318969820256,443.407200506193,443.495439124917,443.583707045765,
443.672075346406,443.760503157567,443.84906129367,443.873307029938,443.961859182017,
444.05029657754,444.138643020738,444.230440353822,444.318684475728,444.406915161664,
444.495153780388,444.583421701236,444.671790001877,444.760217813038,444.84877594914,
444.87302168541,444.96157383749,445.050011233013,445.138357676211,445.230155009295,
445.318399131201,445.406629817137,445.49486843586,445.583136356709,445.67150465735,
445.759932468511,445.848490604614,445.872736340883,445.961288492963,446.049725888486,
446.138072331684,446.229869664768,446.318113786674,446.406344472611,446.494583091335,
446.582851012184,446.671219312825,446.759647123986,446.848205260089,446.872450996356,
446.975474402535,447.078039594968,447.179778915401,447.216201778632),
 .UNSPECIFIED.);
#381=B_SPLINE_CURVE_WITH_KNOTS('',3,(#60750,#60751,#60752,#60753,#60754,
#60755,#60756,#60757,#60758,#60759),.UNSPECIFIED.,.F.,.F.,(4,1,1,1,1,1,
1,4),(447.216202020663,447.872165651829,448.871880307302,449.871594962775,
450.871309618247,451.87102427372,452.870738929193,453.499387327842),
 .UNSPECIFIED.);
#382=B_SPLINE_CURVE_WITH_KNOTS('',3,(#60761,#60762,#60763,#60764,#60765,
#60766,#60767,#60768,#60769,#60770),.UNSPECIFIED.,.F.,.F.,(4,1,1,1,1,1,
1,4),(453.499387327842,453.870453584666,454.870168240139,455.869882895612,
456.869597551084,457.869312206557,458.86902686203,459.782563940701),
 .UNSPECIFIED.);
#383=B_SPLINE_CURVE_WITH_KNOTS('',3,(#60772,#60773,#60774,#60775,#60776,
#60777,#60778,#60779,#60780,#60781,#60782,#60783,#60784,#60785,#60786,#60787,
#60788,#60789,#60790,#60791,#60792,#60793,#60794,#60795,#60796,#60797,#60798,
#60799,#60800,#60801,#60802,#60803,#60804,#60805,#60806,#60807,#60808,#60809,
#60810,#60811,#60812,#60813,#60814,#60815,#60816,#60817,#60818,#60819,#60820,
#60821,#60822,#60823,#60824,#60825,#60826,#60827,#60828,#60829,#60830,#60831,
#60832,#60833,#60834,#60835,#60836,#60837,#60838,#60839,#60840,#60841,#60842,
#60843,#60844,#60845,#60846,#60847,#60848,#60849,#60850,#60851,#60852,#60853,
#60854,#60855,#60856,#60857,#60858,#60859,#60860,#60861,#60862,#60863,#60864,
#60865,#60866,#60867,#60868,#60869,#60870,#60871,#60872,#60873,#60874,#60875,
#60876,#60877,#60878,#60879,#60880,#60881,#60882,#60883,#60884,#60885,#60886,
#60887,#60888,#60889,#60890,#60891,#60892,#60893,#60894,#60895,#60896,#60897,
#60898,#60899,#60900,#60901,#60902,#60903,#60904,#60905,#60906,#60907,#60908,
#60909,#60910,#60911,#60912,#60913,#60914,#60915,#60916,#60917,#60918,#60919,
#60920,#60921,#60922,#60923,#60924,#60925,#60926,#60927,#60928,#60929,#60930,
#60931,#60932,#60933,#60934,#60935,#60936,#60937,#60938,#60939,#60940,#60941,
#60942,#60943,#60944,#60945,#60946,#60947,#60948,#60949,#60950,#60951,#60952,
#60953,#60954,#60955,#60956,#60957,#60958,#60959,#60960,#60961,#60962,#60963,
#60964,#60965,#60966,#60967,#60968,#60969,#60970,#60971,#60972,#60973,#60974,
#60975,#60976,#60977,#60978,#60979,#60980,#60981,#60982,#60983,#60984,#60985,
#60986,#60987,#60988,#60989,#60990,#60991,#60992,#60993,#60994,#60995,#60996,
#60997),.UNSPECIFIED.,.F.,.F.,(4,3,3,3,3,3,3,3,3,3,3,3,3,3,3,3,3,3,3,3,
3,3,3,3,3,3,3,3,3,3,3,3,3,3,3,3,3,3,3,3,3,3,3,3,3,3,3,3,3,3,3,3,3,3,3,3,
3,3,3,3,3,3,3,3,3,3,3,3,3,3,3,3,3,3,3,4),(459.782572635022,459.868741517503,
459.957293669583,460.045731065107,460.134077508305,460.225874841389,460.314118963296,
460.402349649232,460.490588267957,460.578856188805,460.667224489447,460.755652300609,
460.844210436712,460.868456172976,460.957008325056,461.045445720579,461.133792163777,
461.225589496861,461.313833618767,461.402064304703,461.490302923427,461.578570844275,
461.666939144917,461.755366956078,461.84392509218,461.868170828449,461.956722980528,
462.045160376051,462.133506819249,462.225304152333,462.313548274239,462.401778960175,
462.490017578899,462.578285499747,462.666653800388,462.755081611548,462.843639747651,
462.867885483921,462.956437636001,463.044875031524,463.133221474722,463.225018807806,
463.313262929712,463.401493615648,463.489732234372,463.57800015522,463.666368455862,
463.754796267023,463.843354403125,463.867600139394,463.956152291474,464.044589686997,
464.132936130195,464.224733463279,464.312977585185,464.401208271122,464.489446889846,
464.577714810694,464.666083111336,464.754510922497,464.8430690586,464.867314794867,
464.955866946947,465.04430434247,465.132650785668,465.224448118752,465.312692240658,
465.400922926594,465.489161545318,465.577429466167,465.665797766808,465.754225577969,
465.842783714072,465.86702945034,465.994547578253,466.065757942201),
 .UNSPECIFIED.);
#384=B_SPLINE_CURVE_WITH_KNOTS('',3,(#60999,#61000,#61001,#61002,#61003,
#61004,#61005,#61006,#61007,#61008),.UNSPECIFIED.,.F.,.F.,(4,1,1,1,1,1,
1,4),(466.065761334688,466.866744105813,467.866458761286,468.866173416758,
469.865888072231,470.865602727704,471.865317383177,472.348943249381),
 .UNSPECIFIED.);
#385=B_SPLINE_CURVE_WITH_KNOTS('',3,(#61010,#61011,#61012,#61013,#61014,
#61015,#61016,#61017,#61018,#61019),.UNSPECIFIED.,.F.,.F.,(4,1,1,1,1,1,
1,4),(472.348943249381,472.86503203865,473.864746694123,474.864461349595,
475.864176005068,476.863890660541,477.863605316014,478.632128556561),
 .UNSPECIFIED.);
#386=B_SPLINE_CURVE_WITH_KNOTS('',3,(#61021,#61022,#61023,#61024,#61025,
#61026,#61027,#61028,#61029,#61030,#61031),.UNSPECIFIED.,.F.,.F.,(4,1,1,
1,1,1,1,1,4),(478.632128556561,478.863319971487,479.86303462696,480.862749282432,
481.862463937905,482.862178593378,483.861893248851,484.861607904324,484.91531386374),
 .UNSPECIFIED.);
#387=B_SPLINE_CURVE_WITH_KNOTS('',3,(#61033,#61034,#61035,#61036,#61037,
#61038,#61039,#61040,#61041,#61042),.UNSPECIFIED.,.F.,.F.,(4,1,1,1,1,1,
1,4),(484.91531386374,485.861322559797,486.861037215269,487.860751870742,
488.860466526215,489.860181181688,490.859895837161,491.198491737937),
 .UNSPECIFIED.);
#388=B_SPLINE_CURVE_WITH_KNOTS('',3,(#61044,#61045,#61046,#61047,#61048,
#61049,#61050,#61051,#61052,#61053,#61054,#61055,#61056,#61057,#61058,#61059,
#61060,#61061,#61062,#61063,#61064,#61065,#61066,#61067,#61068,#61069,#61070,
#61071,#61072,#61073,#61074,#61075,#61076,#61077,#61078,#61079,#61080,#61081,
#61082,#61083,#61084,#61085,#61086,#61087,#61088,#61089,#61090,#61091,#61092,
#61093,#61094,#61095,#61096,#61097,#61098,#61099,#61100,#61101,#61102,#61103,
#61104,#61105,#61106,#61107,#61108,#61109,#61110,#61111,#61112,#61113,#61114,
#61115,#61116,#61117,#61118,#61119,#61120,#61121,#61122,#61123,#61124,#61125,
#61126,#61127,#61128,#61129,#61130,#61131,#61132,#61133,#61134,#61135,#61136,
#61137,#61138,#61139,#61140,#61141,#61142,#61143,#61144,#61145,#61146,#61147,
#61148,#61149,#61150,#61151,#61152,#61153,#61154,#61155,#61156,#61157,#61158,
#61159,#61160,#61161,#61162,#61163,#61164,#61165,#61166,#61167,#61168,#61169,
#61170,#61171,#61172,#61173,#61174,#61175,#61176,#61177,#61178,#61179,#61180,
#61181,#61182,#61183,#61184,#61185,#61186,#61187,#61188,#61189,#61190,#61191,
#61192,#61193,#61194,#61195,#61196,#61197,#61198,#61199,#61200,#61201,#61202,
#61203,#61204,#61205,#61206,#61207,#61208,#61209,#61210,#61211,#61212,#61213,
#61214,#61215,#61216,#61217,#61218,#61219,#61220,#61221,#61222,#61223,#61224,
#61225,#61226,#61227,#61228,#61229,#61230,#61231,#61232,#61233,#61234,#61235,
#61236,#61237,#61238,#61239,#61240,#61241,#61242,#61243,#61244,#61245,#61246,
#61247,#61248,#61249,#61250,#61251,#61252,#61253,#61254,#61255,#61256,#61257,
#61258,#61259,#61260,#61261,#61262,#61263,#61264,#61265,#61266,#61267,#61268,
#61269),.UNSPECIFIED.,.F.,.F.,(4,3,3,3,3,3,3,3,3,3,3,3,3,3,3,3,3,3,3,3,
3,3,3,3,3,3,3,3,3,3,3,3,3,3,3,3,3,3,3,3,3,3,3,3,3,3,3,3,3,3,3,3,3,3,3,3,
3,3,3,3,3,3,3,3,3,3,3,3,3,3,3,3,3,3,3,4),(491.19849917092,491.286759424022,
491.375007955342,491.463266018858,491.551554870329,491.639950591653,491.728406737234,
491.817005364184,491.859610492634,491.948162644713,492.036600040236,492.124946483433,
492.216743816518,492.304987938423,492.393218624359,492.481457243083,492.56972516393,
492.658093464571,492.746521275732,492.835079411834,492.859325148106,492.947877300185,
493.036314695709,493.124661138907,493.216458471991,493.304702593897,493.392933279833,
493.481171898557,493.569439819405,493.657808120046,493.746235931207,493.83479406731,
493.859039803579,493.947591955659,494.036029351183,494.124375794381,494.216173127465,
494.304417249372,494.392647935309,494.480886554033,494.569154474882,494.657522775524,
494.745950586686,494.834508722789,494.858754459052,494.947306611131,495.035744006654,
495.124090449852,495.215887782936,495.304131904842,495.392362590778,495.480601209502,
495.56886913035,495.657237430991,495.745665242152,495.834223378255,495.858469114525,
495.947021266604,496.035458662126,496.123805105323,496.215602438408,496.303846560313,
496.392077246248,496.480315864971,496.568583785819,496.65695208646,496.74537989762,
496.833938033722,496.858183769998,496.947491550541,497.036679717588,497.125768784926,
497.214770005954,497.303718316016,497.392701397058,497.481684478099),
 .UNSPECIFIED.);
#389=B_SPLINE_CURVE_WITH_KNOTS('',3,(#61271,#61272,#61273,#61274,#61275,
#61276,#61277,#61278,#61279,#61280),.UNSPECIFIED.,.F.,.F.,(4,1,1,1,1,1,
1,4),(497.481692099559,497.857898425471,498.857613080943,499.857327736416,
500.857042391889,501.856757047362,502.856471702835,503.76486095827),
 .UNSPECIFIED.);
#390=B_SPLINE_CURVE_WITH_KNOTS('',3,(#61282,#61283,#61284,#61285,#61286,
#61287,#61288,#61289,#61290,#61291,#61292,#61293,#61294,#61295,#61296,#61297,
#61298,#61299,#61300,#61301,#61302,#61303,#61304,#61305,#61306,#61307,#61308,
#61309,#61310,#61311,#61312,#61313,#61314,#61315,#61316,#61317,#61318,#61319,
#61320,#61321,#61322,#61323,#61324,#61325,#61326,#61327,#61328,#61329,#61330,
#61331,#61332,#61333,#61334,#61335,#61336,#61337,#61338,#61339,#61340,#61341,
#61342,#61343,#61344,#61345,#61346,#61347,#61348,#61349,#61350,#61351,#61352,
#61353,#61354,#61355,#61356,#61357,#61358,#61359,#61360,#61361,#61362,#61363,
#61364,#61365,#61366,#61367,#61368,#61369,#61370,#61371,#61372,#61373,#61374,
#61375,#61376,#61377,#61378,#61379,#61380,#61381,#61382,#61383,#61384,#61385,
#61386,#61387,#61388,#61389,#61390,#61391,#61392,#61393,#61394,#61395,#61396,
#61397,#61398,#61399,#61400,#61401,#61402,#61403,#61404,#61405,#61406,#61407,
#61408,#61409,#61410,#61411,#61412,#61413,#61414,#61415,#61416,#61417,#61418,
#61419,#61420,#61421,#61422,#61423,#61424,#61425,#61426,#61427,#61428,#61429,
#61430,#61431,#61432,#61433,#61434,#61435,#61436,#61437,#61438,#61439,#61440,
#61441,#61442,#61443,#61444,#61445,#61446,#61447,#61448,#61449,#61450,#61451,
#61452,#61453,#61454,#61455,#61456,#61457,#61458,#61459,#61460,#61461,#61462,
#61463,#61464,#61465,#61466,#61467,#61468,#61469,#61470,#61471,#61472,#61473,
#61474,#61475,#61476,#61477,#61478,#61479,#61480,#61481,#61482,#61483,#61484,
#61485,#61486,#61487,#61488,#61489,#61490,#61491,#61492,#61493,#61494,#61495,
#61496,#61497,#61498,#61499,#61500,#61501,#61502,#61503,#61504,#61505,#61506,
#61507),.UNSPECIFIED.,.F.,.F.,(4,3,3,3,3,3,3,3,3,3,3,3,3,3,3,3,3,3,3,3,
3,3,3,3,3,3,3,3,3,3,3,3,3,3,3,3,3,3,3,3,3,3,3,3,3,3,3,3,3,3,3,3,3,3,3,3,
3,3,3,3,3,3,3,3,3,3,3,3,3,3,3,3,3,3,3,4),(503.764869785279,503.856186358308,
503.944738510238,504.033175905611,504.12152234866,504.2133196818,504.30156380356,
504.38979448935,504.47803310793,504.566301028635,504.654669329136,504.743097140158,
504.831655276124,504.85590101378,504.94445316576,505.032890561183,505.121237004278,
505.2130343374,505.301278459201,505.38950914503,505.477747763647,505.566015684387,
505.654383984919,505.742811795971,505.831369931965,505.855615669253,505.944167822066,
506.032605218325,506.120951662261,506.212748995069,506.30099311771,506.38922380438,
506.477462423835,506.565730345411,506.654098646772,506.742526458648,506.831084595454,
506.855330324726,506.943882475663,507.032319870044,507.120666312104,507.212463645616,
507.300707766398,507.388938451218,507.477177068833,507.565444988583,507.653813288145,
507.742241098236,507.830799233292,507.855044980199,507.943597131997,508.032034527227,
508.120380970122,508.212178303315,508.300422424894,508.388653110495,508.476891728876,
508.565159649373,508.653527949655,508.74195576045,508.830513896182,508.854759635672,
508.943311792402,509.031749192592,509.120095640468,509.211892971802,509.300137098383,
509.388367788985,509.476606412361,509.564874337843,509.653242643066,509.741670458786,
509.830228599376,509.854474291144,509.983739743113,510.048055092458),
 .UNSPECIFIED.);
#391=B_SPLINE_CURVE_WITH_KNOTS('',3,(#61509,#61510,#61511,#61512,#61513,
#61514,#61515,#61516,#61517,#61518),.UNSPECIFIED.,.F.,.F.,(4,1,1,1,1,1,
1,4),(510.048058981494,510.854188946617,511.85390360209,512.853618257563,
513.853332913036,514.853047568509,515.852762223982,516.331240399638),
 .UNSPECIFIED.);
#392=B_SPLINE_CURVE_WITH_KNOTS('',3,(#61520,#61521,#61522,#61523,#61524,
#61525,#61526,#61527,#61528,#61529),.UNSPECIFIED.,.F.,.F.,(4,1,1,1,1,1,
1,4),(516.331240399638,516.852476879454,517.852191534927,518.8519061904,
519.851620845873,520.851335501346,521.851050156819,522.614425706818),
 .UNSPECIFIED.);
#393=B_SPLINE_CURVE_WITH_KNOTS('',3,(#61531,#61532,#61533,#61534,#61535,
#61536,#61537,#61538,#61539,#61540,#61541,#61542,#61543,#61544,#61545,#61546,
#61547,#61548,#61549,#61550,#61551,#61552,#61553,#61554,#61555,#61556,#61557,
#61558,#61559,#61560,#61561,#61562,#61563,#61564,#61565,#61566,#61567,#61568,
#61569,#61570,#61571,#61572,#61573,#61574,#61575,#61576,#61577,#61578,#61579,
#61580,#61581,#61582,#61583,#61584,#61585,#61586,#61587,#61588,#61589,#61590,
#61591,#61592,#61593,#61594,#61595,#61596,#61597,#61598,#61599,#61600,#61601,
#61602,#61603,#61604,#61605,#61606,#61607,#61608,#61609,#61610,#61611,#61612,
#61613,#61614,#61615,#61616,#61617,#61618,#61619,#61620,#61621,#61622,#61623,
#61624,#61625,#61626,#61627,#61628,#61629,#61630,#61631,#61632,#61633,#61634,
#61635,#61636,#61637,#61638,#61639,#61640,#61641,#61642,#61643,#61644,#61645,
#61646,#61647,#61648,#61649,#61650,#61651,#61652,#61653,#61654,#61655,#61656,
#61657,#61658,#61659,#61660,#61661,#61662,#61663,#61664,#61665,#61666,#61667,
#61668,#61669,#61670,#61671,#61672,#61673,#61674,#61675,#61676,#61677,#61678,
#61679,#61680,#61681,#61682,#61683,#61684,#61685,#61686,#61687,#61688,#61689,
#61690,#61691,#61692,#61693,#61694,#61695,#61696,#61697,#61698,#61699,#61700,
#61701,#61702,#61703,#61704,#61705,#61706,#61707,#61708,#61709,#61710,#61711,
#61712,#61713,#61714),.UNSPECIFIED.,.F.,.F.,(4,3,3,3,3,3,3,3,3,3,3,3,3,
3,3,3,3,3,3,3,3,3,3,3,3,3,3,3,3,3,3,3,3,3,3,3,3,3,3,3,3,3,3,3,3,3,3,3,3,
3,3,3,3,3,3,3,3,3,3,3,3,4),(522.614425731277,522.732595271784,522.850764812291,
522.939338841653,523.027798028275,523.116166152673,523.207955317059,523.296220715231,
523.384472493103,523.472731997983,523.561020577581,523.649409097732,523.737856897892,
523.826434531246,523.850479467764,523.939059065491,524.027524204539,524.115898653165,
524.207685586924,524.295958186708,524.384217475473,524.472484790942,524.560781471458,
524.649178477884,524.737634998707,524.826221625929,524.850194123237,524.938612611537,
525.026916056542,525.115128415847,525.206975961205,525.295086481409,525.383183961474,
525.471289905623,525.559425819224,525.647663761157,525.735962006623,525.824392749395,
525.84990877871,525.938637365966,526.02725073032,526.115772475931,526.207503845712,
526.295920522753,526.384322455804,526.472730833281,526.561166842936,526.649699920224,
526.738290777186,526.827008176059,526.849623434183,526.93745568206,527.025175697194,
527.112808046017,527.200379484124,527.287919497547,527.375450147699,527.462993483972,
527.550623210395,527.638298940645,527.726108902286,527.787264933936),
 .UNSPECIFIED.);
#394=B_SPLINE_CURVE_WITH_KNOTS('',3,(#61718,#61719,#61720,#61721,#61722,
#61723,#61724,#61725),.UNSPECIFIED.,.F.,.F.,(4,1,1,1,1,4),(-529.848767400601,
-528.849052745128,-527.849338089655,-526.849623434182,-525.84990877871,
-525.597129536099),.UNSPECIFIED.);
#395=B_SPLINE_CURVE_WITH_KNOTS('',3,(#61727,#61728,#61729,#61730,#61731,
#61732,#61733,#61734,#61735,#61736),.UNSPECIFIED.,.F.,.F.,(4,1,1,1,1,1,
1,4),(-525.597129536099,-524.850194123237,-523.850479467764,-522.850764812291,
-521.851050156818,-520.851335501345,-519.851620845873,-519.313944228919),
 .UNSPECIFIED.);
#396=B_SPLINE_CURVE_WITH_KNOTS('',3,(#61738,#61739,#61740,#61741,#61742,
#61743,#61744,#61745,#61746,#61747,#61748,#61749,#61750,#61751,#61752,#61753,
#61754,#61755,#61756,#61757,#61758,#61759,#61760,#61761,#61762,#61763,#61764,
#61765,#61766,#61767,#61768,#61769,#61770,#61771,#61772,#61773,#61774,#61775,
#61776,#61777,#61778,#61779,#61780,#61781,#61782,#61783,#61784,#61785,#61786,
#61787,#61788,#61789,#61790,#61791,#61792,#61793,#61794,#61795,#61796,#61797,
#61798,#61799,#61800,#61801,#61802,#61803,#61804,#61805,#61806,#61807,#61808,
#61809,#61810,#61811,#61812,#61813,#61814,#61815,#61816,#61817,#61818,#61819,
#61820,#61821,#61822,#61823,#61824,#61825,#61826,#61827,#61828,#61829,#61830,
#61831,#61832,#61833,#61834,#61835,#61836,#61837,#61838,#61839,#61840,#61841,
#61842,#61843,#61844,#61845,#61846,#61847,#61848,#61849,#61850,#61851,#61852,
#61853,#61854,#61855,#61856,#61857,#61858,#61859,#61860,#61861,#61862,#61863,
#61864,#61865,#61866,#61867,#61868,#61869,#61870,#61871,#61872,#61873,#61874,
#61875,#61876,#61877,#61878,#61879,#61880,#61881,#61882,#61883,#61884,#61885,
#61886,#61887,#61888,#61889,#61890,#61891,#61892,#61893,#61894,#61895,#61896,
#61897,#61898,#61899,#61900,#61901,#61902,#61903,#61904,#61905,#61906,#61907,
#61908,#61909,#61910,#61911,#61912,#61913,#61914,#61915,#61916,#61917,#61918,
#61919,#61920,#61921,#61922,#61923,#61924,#61925,#61926,#61927,#61928,#61929,
#61930,#61931,#61932,#61933,#61934,#61935,#61936,#61937,#61938,#61939,#61940,
#61941,#61942,#61943,#61944,#61945,#61946,#61947,#61948,#61949,#61950,#61951,
#61952,#61953,#61954,#61955,#61956,#61957,#61958,#61959,#61960,#61961,#61962,
#61963),.UNSPECIFIED.,.F.,.F.,(4,3,3,3,3,3,3,3,3,3,3,3,3,3,3,3,3,3,3,3,
3,3,3,3,3,3,3,3,3,3,3,3,3,3,3,3,3,3,3,3,3,3,3,3,3,3,3,3,3,3,3,3,3,3,3,3,
3,3,3,3,3,3,3,3,3,3,3,3,3,3,3,3,3,3,3,4),(-519.313944022838,-519.219926438778,
-519.125587303341,-519.031086436992,-518.936299770552,-518.8519061904,-518.763353055329,
-518.674914668526,-518.586567226996,-518.494770265487,-518.406525133958,
-518.318293435948,-518.230053803774,-518.141784869172,-518.053415559458,
-517.964986740699,-517.876427606999,-517.852191534927,-517.763639159473,
-517.675201534523,-517.586854856148,-517.495057609062,-517.40681323902,
-517.318582300568,-517.230343425196,-517.142075243814,-517.053706678148,
-516.965278599017,-516.876720192668,-516.852476879454,-516.763925130966,
-516.675488144823,-516.587142116275,-516.495344629738,-516.407100933068,
-516.318870675562,-516.23063248802,-516.142365000663,-516.053997134773,
-515.965569759635,-515.877012058054,-515.852762223981,-515.764209903475,
-515.675772337909,-515.587425723263,-515.495628453919,-515.407384158139,
-515.319153297728,-515.230914504112,-515.14264640814,-515.054277932913,
-514.965849947264,-514.877291638172,-514.853047568508,-514.764495399659,
-514.676057986669,-514.58771152533,-514.495914198794,-514.407670057167,
-514.319439350958,-514.231200711427,-514.142932769258,-514.054564446634,
-513.966136613078,-513.877578454143,-513.853332913036,-513.766099848692,
-513.678981063572,-513.591962273271,-513.504998644919,-513.418067626277,
-513.331146700021,-513.244177277615,-513.157180490533,-513.070089141411,
-513.03075892174),.UNSPECIFIED.);
#397=B_SPLINE_CURVE_WITH_KNOTS('',3,(#61965,#61966,#61967,#61968,#61969,
#61970,#61971,#61972,#61973,#61974,#61975),.UNSPECIFIED.,.F.,.F.,(4,1,1,
1,1,1,1,1,4),(-513.03075892174,-512.853618257563,-511.85390360209,-510.854188946617,
-509.854474291144,-508.854759635672,-507.855044980199,-506.855330324726,
-506.74757361456),.UNSPECIFIED.);
#398=B_SPLINE_CURVE_WITH_KNOTS('',3,(#61977,#61978,#61979,#61980,#61981,
#61982,#61983,#61984,#61985,#61986),.UNSPECIFIED.,.F.,.F.,(4,1,1,1,1,1,
1,4),(-506.74757361456,-505.855615669253,-504.85590101378,-503.856186358307,
-502.856471702834,-501.856757047362,-500.857042391889,-500.46438830738),
 .UNSPECIFIED.);
#399=B_SPLINE_CURVE_WITH_KNOTS('',3,(#61988,#61989,#61990,#61991,#61992,
#61993,#61994,#61995,#61996,#61997),.UNSPECIFIED.,.F.,.F.,(4,1,1,1,1,1,
1,4),(-500.46438830738,-499.857327736416,-498.857613080943,-497.85789842547,
-496.858183769998,-495.858469114525,-494.858754459052,-494.181203000201),
 .UNSPECIFIED.);
#400=B_SPLINE_CURVE_WITH_KNOTS('',3,(#61999,#62000,#62001,#62002,#62003,
#62004,#62005,#62006,#62007,#62008),.UNSPECIFIED.,.F.,.F.,(4,1,1,1,1,1,
1,4),(-494.181203000201,-493.859039803579,-492.859325148106,-491.859610492633,
-490.859895837161,-489.860181181688,-488.860466526215,-487.898022689968),
 .UNSPECIFIED.);
#401=B_SPLINE_CURVE_WITH_KNOTS('',3,(#62010,#62011,#62012,#62013,#62014,
#62015,#62016,#62017,#62018,#62019,#62020,#62021,#62022,#62023,#62024,#62025,
#62026,#62027,#62028,#62029,#62030,#62031,#62032,#62033,#62034,#62035,#62036,
#62037,#62038,#62039,#62040,#62041,#62042,#62043,#62044,#62045,#62046,#62047,
#62048,#62049,#62050,#62051,#62052,#62053,#62054,#62055,#62056,#62057,#62058,
#62059,#62060,#62061,#62062,#62063,#62064,#62065,#62066,#62067,#62068,#62069,
#62070,#62071,#62072,#62073,#62074,#62075,#62076,#62077,#62078,#62079,#62080,
#62081,#62082,#62083,#62084,#62085,#62086,#62087,#62088,#62089,#62090,#62091,
#62092,#62093,#62094,#62095,#62096,#62097,#62098,#62099,#62100,#62101,#62102,
#62103,#62104,#62105,#62106,#62107,#62108,#62109,#62110,#62111,#62112,#62113,
#62114,#62115,#62116,#62117,#62118,#62119,#62120,#62121,#62122,#62123,#62124,
#62125,#62126,#62127,#62128,#62129,#62130,#62131,#62132,#62133,#62134,#62135,
#62136,#62137,#62138,#62139,#62140,#62141,#62142,#62143,#62144,#62145,#62146,
#62147,#62148,#62149,#62150,#62151,#62152,#62153,#62154,#62155,#62156,#62157,
#62158,#62159,#62160,#62161,#62162,#62163,#62164,#62165,#62166,#62167,#62168,
#62169,#62170,#62171,#62172,#62173,#62174,#62175,#62176,#62177,#62178,#62179,
#62180,#62181,#62182,#62183,#62184,#62185,#62186,#62187,#62188,#62189,#62190,
#62191,#62192,#62193,#62194,#62195,#62196,#62197,#62198,#62199,#62200,#62201,
#62202,#62203,#62204,#62205,#62206,#62207,#62208,#62209,#62210,#62211,#62212,
#62213,#62214,#62215,#62216,#62217,#62218,#62219,#62220,#62221,#62222,#62223,
#62224,#62225,#62226,#62227,#62228,#62229,#62230,#62231,#62232,#62233,#62234,
#62235,#62236,#62237,#62238),.UNSPECIFIED.,.F.,.F.,(4,3,3,3,3,3,3,3,3,3,
3,3,3,3,3,3,3,3,3,3,3,3,3,3,3,3,3,3,3,3,3,3,3,3,3,3,3,3,3,3,3,3,3,3,3,3,
3,3,3,3,3,3,3,3,3,3,3,3,3,3,3,3,3,3,3,3,3,3,3,3,3,3,3,3,3,3,4),(-487.898017693021,
-487.860751870742,-487.772199718662,-487.683762323139,-487.595415879941,
-487.503618546857,-487.415374424951,-487.327143739015,-487.238905120291,
-487.150637199442,-487.062268898801,-486.97384108764,-486.885282951537,
-486.861037215269,-486.772485063189,-486.684047667666,-486.595701224468,
-486.503903891384,-486.415659769478,-486.327429083542,-486.239190464818,
-486.15092254397,-486.062554243328,-485.974126432167,-485.885568296064,
-485.861322559796,-485.772770407716,-485.684333012193,-485.595986568995,
-485.504189235911,-485.415945114005,-485.327714428068,-485.239475809344,
-485.151207888496,-485.062839587855,-484.974411776693,-484.885853640591,
-484.861607904323,-484.773055752244,-484.684618356721,-484.596271913523,
-484.504474580439,-484.416230458533,-484.327999772597,-484.239761153874,
-484.151493233026,-484.063124932385,-483.974697121224,-483.886138985121,
-483.861893248851,-483.773341096771,-483.684903701248,-483.59655725805,
-483.504759924966,-483.41651580306,-483.328285117124,-483.2400464984,-483.151778577551,
-483.06341027691,-482.974982465749,-482.886424329646,-482.862178593378,
-482.773626441298,-482.685189045775,-482.596842602576,-482.505045269492,
-482.416801147586,-482.32857046165,-482.240331842926,-482.152063922077,
-482.063695621436,-481.975267810275,-481.886709674172,-481.862463937905,
-481.745859209655,-481.631952730172,-481.614832480211),.UNSPECIFIED.);
#402=B_SPLINE_CURVE_WITH_KNOTS('',3,(#62240,#62241,#62242,#62243,#62244,
#62245,#62246,#62247,#62248,#62249),.UNSPECIFIED.,.F.,.F.,(4,1,1,1,1,1,
1,4),(-481.614832385842,-480.862749282432,-479.863034626959,-478.863319971486,
-477.863605316014,-476.863890660541,-475.864176005068,-475.331647078662),
 .UNSPECIFIED.);
#403=B_SPLINE_CURVE_WITH_KNOTS('',3,(#62251,#62252,#62253,#62254,#62255,
#62256,#62257,#62258,#62259,#62260),.UNSPECIFIED.,.F.,.F.,(4,1,1,1,1,1,
1,4),(-475.331647078662,-474.864461349595,-473.864746694122,-472.86503203865,
-471.865317383177,-470.865602727704,-469.865888072231,-469.048461771483),
 .UNSPECIFIED.);
#404=B_SPLINE_CURVE_WITH_KNOTS('',3,(#62262,#62263,#62264,#62265,#62266,
#62267,#62268,#62269,#62270,#62271,#62272),.UNSPECIFIED.,.F.,.F.,(4,1,1,
1,1,1,1,1,4),(-469.048461771483,-468.866173416758,-467.866458761285,-466.866744105813,
-465.86702945034,-464.867314794867,-463.867600139394,-462.867885483921,
-462.765276464303),.UNSPECIFIED.);
#405=B_SPLINE_CURVE_WITH_KNOTS('',3,(#62274,#62275,#62276,#62277,#62278,
#62279,#62280,#62281,#62282,#62283),.UNSPECIFIED.,.F.,.F.,(4,1,1,1,1,1,
1,4),(-462.765276464303,-461.868170828448,-460.868456172976,-459.868741517503,
-458.86902686203,-457.869312206557,-456.869597551084,-456.482098551466),
 .UNSPECIFIED.);
#406=B_SPLINE_CURVE_WITH_KNOTS('',3,(#62285,#62286,#62287,#62288,#62289,
#62290,#62291,#62292,#62293,#62294,#62295,#62296,#62297,#62298,#62299,#62300,
#62301,#62302,#62303,#62304,#62305,#62306,#62307,#62308,#62309,#62310,#62311,
#62312,#62313,#62314,#62315,#62316,#62317,#62318,#62319,#62320,#62321,#62322,
#62323,#62324,#62325,#62326,#62327,#62328,#62329,#62330,#62331,#62332,#62333,
#62334,#62335,#62336,#62337,#62338,#62339,#62340,#62341,#62342,#62343,#62344,
#62345,#62346,#62347,#62348,#62349,#62350,#62351,#62352,#62353,#62354,#62355,
#62356,#62357,#62358,#62359,#62360,#62361,#62362,#62363,#62364,#62365,#62366,
#62367,#62368,#62369,#62370,#62371,#62372,#62373,#62374,#62375,#62376,#62377,
#62378,#62379,#62380,#62381,#62382,#62383,#62384,#62385,#62386,#62387,#62388,
#62389,#62390,#62391,#62392,#62393,#62394,#62395,#62396,#62397,#62398,#62399,
#62400,#62401,#62402,#62403,#62404,#62405,#62406,#62407,#62408,#62409,#62410,
#62411,#62412,#62413,#62414,#62415,#62416,#62417,#62418,#62419,#62420,#62421,
#62422,#62423,#62424,#62425,#62426,#62427,#62428,#62429,#62430,#62431,#62432,
#62433,#62434,#62435,#62436,#62437,#62438,#62439,#62440,#62441,#62442,#62443,
#62444,#62445,#62446,#62447,#62448,#62449,#62450,#62451,#62452,#62453,#62454,
#62455,#62456,#62457,#62458,#62459,#62460,#62461,#62462,#62463,#62464,#62465,
#62466,#62467,#62468,#62469,#62470,#62471,#62472,#62473,#62474,#62475,#62476,
#62477,#62478,#62479,#62480,#62481,#62482,#62483,#62484,#62485,#62486,#62487,
#62488,#62489,#62490,#62491,#62492,#62493,#62494,#62495,#62496,#62497,#62498,
#62499,#62500,#62501,#62502,#62503,#62504,#62505,#62506,#62507,#62508,#62509,
#62510),.UNSPECIFIED.,.F.,.F.,(4,3,3,3,3,3,3,3,3,3,3,3,3,3,3,3,3,3,3,3,
3,3,3,3,3,3,3,3,3,3,3,3,3,3,3,3,3,3,3,3,3,3,3,3,3,3,3,3,3,3,3,3,3,3,3,3,
3,3,3,3,3,3,3,3,3,3,3,3,3,3,3,3,3,3,3,4),(-456.482091157123,-456.39293905207,
-456.303770120477,-456.214564491945,-456.12523803452,-456.035848798725,
-455.946295126569,-455.869882895611,-455.781330743532,-455.692893348009,
-455.604546904811,-455.512749571727,-455.424505449821,-455.336274763885,
-455.248036145161,-455.159768224313,-455.071399923672,-454.982972112511,
-454.894413976409,-454.870168240139,-454.781616088059,-454.693178692536,
-454.604832249338,-454.513034916254,-454.424790794348,-454.336560108412,
-454.248321489688,-454.160053568839,-454.071685268198,-453.983257457037,
-453.894699320934,-453.870453584666,-453.781901432586,-453.693464037063,
-453.605117593865,-453.513320260781,-453.425076138875,-453.336845452938,
-453.248606834214,-453.160338913365,-453.071970612724,-452.983542801563,
-452.89498466546,-452.870738929193,-452.782186777114,-452.69374938159,-452.605402938392,
-452.513605605308,-452.425361483402,-452.337130797466,-452.248892178742,
-452.160624257893,-452.072255957252,-451.983828146091,-451.895270009989,
-451.87102427372,-451.78247212164,-451.694034726117,-451.605688282919,-451.513890949835,
-451.425646827929,-451.337416141993,-451.249177523268,-451.160909602419,
-451.072541301778,-450.984113490617,-450.895555354514,-450.871309618247,
-450.782910718183,-450.694622961227,-450.60642468146,-450.518294288706,
-450.430203020071,-450.342135685022,-450.254047585887,-450.198905849944),
 .UNSPECIFIED.);
#407=B_SPLINE_CURVE_WITH_KNOTS('',3,(#62512,#62513,#62514,#62515,#62516,
#62517,#62518,#62519,#62520,#62521),.UNSPECIFIED.,.F.,.F.,(4,1,1,1,1,1,
1,4),(-450.198898760757,-449.871594962774,-448.871880307302,-447.872165651829,
-446.872450996356,-445.872736340883,-444.87302168541,-443.915726084063),
 .UNSPECIFIED.);
#408=B_SPLINE_CURVE_WITH_KNOTS('',3,(#62523,#62524,#62525,#62526,#62527,
#62528,#62529,#62530,#62531,#62532,#62533,#62534,#62535,#62536,#62537,#62538,
#62539,#62540,#62541,#62542,#62543,#62544,#62545,#62546,#62547,#62548,#62549,
#62550,#62551,#62552,#62553,#62554,#62555,#62556,#62557,#62558,#62559,#62560,
#62561,#62562,#62563,#62564,#62565,#62566,#62567,#62568,#62569,#62570,#62571,
#62572,#62573,#62574,#62575,#62576,#62577,#62578,#62579,#62580,#62581,#62582,
#62583,#62584,#62585,#62586,#62587,#62588,#62589,#62590,#62591,#62592,#62593,
#62594,#62595,#62596,#62597,#62598,#62599,#62600,#62601,#62602,#62603,#62604,
#62605,#62606,#62607,#62608,#62609,#62610,#62611,#62612,#62613,#62614,#62615,
#62616,#62617,#62618,#62619,#62620,#62621,#62622,#62623,#62624,#62625,#62626,
#62627,#62628,#62629,#62630,#62631,#62632,#62633,#62634,#62635,#62636,#62637,
#62638,#62639,#62640,#62641,#62642,#62643,#62644,#62645,#62646,#62647,#62648,
#62649,#62650,#62651,#62652,#62653,#62654,#62655,#62656,#62657,#62658,#62659,
#62660,#62661,#62662,#62663,#62664,#62665,#62666,#62667,#62668,#62669,#62670,
#62671,#62672,#62673,#62674,#62675,#62676,#62677,#62678,#62679,#62680,#62681,
#62682,#62683,#62684,#62685,#62686,#62687,#62688,#62689,#62690,#62691,#62692,
#62693,#62694,#62695,#62696,#62697,#62698,#62699,#62700,#62701,#62702,#62703,
#62704,#62705,#62706,#62707,#62708,#62709,#62710,#62711,#62712,#62713,#62714,
#62715,#62716,#62717,#62718,#62719,#62720,#62721,#62722,#62723,#62724,#62725,
#62726,#62727,#62728,#62729,#62730,#62731,#62732,#62733,#62734,#62735,#62736,
#62737,#62738,#62739,#62740,#62741,#62742,#62743,#62744,#62745,#62746,#62747,
#62748,#62749,#62750,#62751),.UNSPECIFIED.,.F.,.F.,(4,3,3,3,3,3,3,3,3,3,
3,3,3,3,3,3,3,3,3,3,3,3,3,3,3,3,3,3,3,3,3,3,3,3,3,3,3,3,3,3,3,3,3,3,3,3,
3,3,3,3,3,3,3,3,3,3,3,3,3,3,3,3,3,3,3,3,3,3,3,3,3,3,3,3,3,3,4),(-443.915720542764,
-443.873307029937,-443.784754877858,-443.696317482335,-443.607971039137,
-443.516173706053,-443.427929584147,-443.339698898211,-443.251460279487,
-443.163192358639,-443.074824057998,-442.986396246837,-442.897838110735,
-442.873592374465,-442.785040222385,-442.696602826862,-442.608256383664,
-442.51645905058,-442.428214928674,-442.339984242738,-442.251745624014,
-442.163477703165,-442.075109402524,-441.986681591363,-441.89812345526,
-441.873877718992,-441.785325566912,-441.696888171389,-441.608541728191,
-441.516744395107,-441.428500273201,-441.340269587264,-441.25203096854,
-441.163763047692,-441.075394747051,-440.986966935889,-440.898408799787,
-440.874163063519,-440.785610911439,-440.697173515916,-440.608827072718,
-440.517029739634,-440.428785617728,-440.340554931792,-440.252316313068,
-440.16404839222,-440.075680091579,-439.987252280418,-439.898694144315,
-439.874448408046,-439.785896255966,-439.697458860443,-439.609112417245,
-439.517315084161,-439.429070962255,-439.340840276319,-439.252601657595,
-439.164333736747,-439.075965436105,-438.987537624944,-438.898979488841,
-438.874733752573,-438.786181600493,-438.69774420497,-438.609397761772,
-438.517600428688,-438.429356306782,-438.341125620845,-438.252887002121,
-438.164619081273,-438.076250780631,-437.98782296947,-437.899264833367,
-437.8750190971,-437.75377719744,-437.639047704226,-437.632535297779),
 .UNSPECIFIED.);
#409=B_SPLINE_CURVE_WITH_KNOTS('',3,(#62753,#62754,#62755,#62756,#62757,
#62758,#62759,#62760,#62761,#62762),.UNSPECIFIED.,.F.,.F.,(4,1,1,1,1,1,
1,4),(-437.632535235585,-436.875304441628,-435.875589786155,-434.875875130682,
-433.876160475209,-432.876445819736,-431.876731164263,-431.349349928405),
 .UNSPECIFIED.);
#410=B_SPLINE_CURVE_WITH_KNOTS('',3,(#62764,#62765,#62766,#62767,#62768,
#62769,#62770,#62771,#62772,#62773),.UNSPECIFIED.,.F.,.F.,(4,1,1,1,1,1,
1,4),(-431.349349928405,-430.877016508791,-429.877301853318,-428.877587197845,
-427.877872542372,-426.878157886899,-425.878443231426,-425.066169088357),
 .UNSPECIFIED.);
#411=B_SPLINE_CURVE_WITH_KNOTS('',3,(#62775,#62776,#62777,#62778,#62779,
#62780,#62781,#62782,#62783,#62784,#62785,#62786,#62787,#62788,#62789,#62790,
#62791,#62792,#62793,#62794,#62795,#62796,#62797,#62798,#62799,#62800,#62801,
#62802,#62803,#62804,#62805,#62806,#62807,#62808,#62809,#62810,#62811,#62812,
#62813,#62814,#62815,#62816,#62817,#62818,#62819,#62820,#62821,#62822,#62823,
#62824,#62825,#62826,#62827,#62828,#62829,#62830,#62831,#62832,#62833,#62834,
#62835,#62836,#62837,#62838,#62839,#62840,#62841,#62842,#62843,#62844,#62845,
#62846,#62847,#62848,#62849,#62850,#62851,#62852,#62853,#62854,#62855,#62856,
#62857,#62858,#62859,#62860,#62861,#62862,#62863,#62864,#62865,#62866,#62867,
#62868,#62869,#62870,#62871,#62872,#62873,#62874,#62875,#62876,#62877,#62878,
#62879,#62880,#62881,#62882,#62883,#62884,#62885,#62886,#62887,#62888,#62889,
#62890,#62891,#62892,#62893,#62894,#62895,#62896,#62897,#62898,#62899,#62900,
#62901,#62902,#62903,#62904,#62905,#62906,#62907,#62908,#62909,#62910,#62911,
#62912,#62913,#62914,#62915,#62916,#62917,#62918,#62919,#62920,#62921,#62922,
#62923,#62924,#62925,#62926,#62927,#62928,#62929,#62930,#62931,#62932,#62933,
#62934,#62935,#62936,#62937,#62938,#62939,#62940,#62941,#62942,#62943,#62944,
#62945,#62946,#62947,#62948,#62949,#62950,#62951,#62952,#62953,#62954,#62955,
#62956,#62957,#62958,#62959,#62960,#62961,#62962,#62963,#62964,#62965,#62966,
#62967,#62968,#62969,#62970,#62971,#62972,#62973,#62974,#62975,#62976,#62977,
#62978,#62979,#62980,#62981,#62982,#62983,#62984,#62985,#62986,#62987,#62988,
#62989,#62990,#62991,#62992,#62993,#62994,#62995,#62996,#62997,#62998,#62999,
#63000),.UNSPECIFIED.,.F.,.F.,(4,3,3,3,3,3,3,3,3,3,3,3,3,3,3,3,3,3,3,3,
3,3,3,3,3,3,3,3,3,3,3,3,3,3,3,3,3,3,3,3,3,3,3,3,3,3,3,3,3,3,3,3,3,3,3,3,
3,3,3,3,3,3,3,3,3,3,3,3,3,3,3,3,3,3,3,4),(-425.066164621226,-424.934650446996,
-424.878728575954,-424.790176423874,-424.701739028351,-424.613392585153,
-424.521595252069,-424.433351130163,-424.345120444227,-424.256881825503,
-424.168613904655,-424.080245604013,-423.991817792852,-423.903259656749,
-423.879013920481,-423.790461768401,-423.702024372878,-423.61367792968,
-423.521880596596,-423.43363647469,-423.345405788754,-423.25716717003,-423.168899249181,
-423.08053094854,-422.992103137379,-422.903545001276,-422.879299265008,
-422.790747112928,-422.702309717405,-422.613963274207,-422.522165941123,
-422.433921819217,-422.345691133281,-422.257452514557,-422.169184593709,
-422.080816293068,-421.992388481907,-421.903830345804,-421.879584609535,
-421.791032457455,-421.702595061932,-421.614248618734,-421.52245128565,
-421.434207163744,-421.345976477808,-421.257737859084,-421.169469938235,
-421.081101637594,-420.992673826433,-420.90411569033,-420.879869954062,
-420.791317801982,-420.702880406459,-420.614533963261,-420.522736630177,
-420.434492508271,-420.346261822334,-420.25802320361,-420.169755282762,
-420.081386982121,-419.992959170959,-419.904401034857,-419.880155298589,
-419.79160314651,-419.703165750987,-419.614819307789,-419.523021974705,
-419.434777852799,-419.346547166863,-419.258308548139,-419.170040627291,
-419.08167232665,-418.993244515489,-418.904686379387,-418.880440643117,
-418.782979314046),.UNSPECIFIED.);
#412=B_SPLINE_CURVE_WITH_KNOTS('',3,(#63002,#63003,#63004,#63005,#63006,
#63007,#63008,#63009,#63010,#63011),.UNSPECIFIED.,.F.,.F.,(4,1,1,1,1,1,
1,4),(-418.782970387294,-417.880725987644,-416.881011332171,-415.881296676698,
-414.881582021225,-413.881867365752,-412.88215271028,-412.499801520433),
 .UNSPECIFIED.);
#413=B_SPLINE_CURVE_WITH_KNOTS('',3,(#63013,#63014,#63015,#63016,#63017,
#63018,#63019,#63020,#63021,#63022,#63023,#63024,#63025,#63026,#63027,#63028,
#63029,#63030,#63031,#63032,#63033,#63034,#63035,#63036,#63037,#63038,#63039,
#63040,#63041,#63042,#63043,#63044,#63045,#63046,#63047,#63048,#63049,#63050,
#63051,#63052,#63053,#63054,#63055,#63056,#63057,#63058,#63059,#63060,#63061,
#63062,#63063,#63064,#63065,#63066,#63067,#63068,#63069,#63070,#63071,#63072,
#63073,#63074,#63075,#63076,#63077,#63078,#63079,#63080,#63081,#63082,#63083,
#63084,#63085,#63086,#63087,#63088,#63089,#63090,#63091,#63092,#63093,#63094,
#63095,#63096,#63097,#63098,#63099,#63100,#63101,#63102,#63103,#63104,#63105,
#63106,#63107,#63108,#63109,#63110,#63111,#63112,#63113,#63114,#63115,#63116,
#63117,#63118,#63119,#63120,#63121,#63122,#63123,#63124,#63125,#63126,#63127,
#63128,#63129,#63130,#63131,#63132,#63133,#63134,#63135,#63136,#63137,#63138,
#63139,#63140,#63141,#63142,#63143,#63144,#63145,#63146,#63147,#63148,#63149,
#63150,#63151,#63152,#63153,#63154,#63155,#63156,#63157,#63158,#63159,#63160,
#63161,#63162,#63163,#63164,#63165,#63166,#63167,#63168,#63169,#63170,#63171,
#63172,#63173,#63174,#63175,#63176,#63177,#63178,#63179,#63180,#63181,#63182,
#63183,#63184,#63185,#63186,#63187,#63188,#63189,#63190,#63191,#63192,#63193,
#63194,#63195,#63196,#63197,#63198,#63199,#63200,#63201,#63202,#63203,#63204,
#63205,#63206,#63207,#63208,#63209,#63210,#63211,#63212,#63213,#63214,#63215,
#63216,#63217,#63218,#63219,#63220,#63221,#63222,#63223,#63224,#63225,#63226,
#63227,#63228,#63229,#63230,#63231,#63232,#63233,#63234,#63235,#63236,#63237,
#63238),.UNSPECIFIED.,.F.,.F.,(4,3,3,3,3,3,3,3,3,3,3,3,3,3,3,3,3,3,3,3,
3,3,3,3,3,3,3,3,3,3,3,3,3,3,3,3,3,3,3,3,3,3,3,3,3,3,3,3,3,3,3,3,3,3,3,3,
3,3,3,3,3,3,3,3,3,3,3,3,3,3,3,3,3,3,3,4),(-412.499794006866,-412.410749231375,
-412.321691006471,-412.232599270962,-412.143389567396,-412.054119542542,
-411.964684583505,-411.882438054807,-411.793885902727,-411.705448507204,
-411.617102064006,-411.525304730922,-411.437060609015,-411.348829923079,
-411.260591304355,-411.172323383506,-411.083955082865,-410.995527271704,
-410.906969135601,-410.882723399334,-410.794171247254,-410.705733851731,
-410.617387408533,-410.525590075449,-410.437345953543,-410.349115267606,
-410.260876648883,-410.172608728035,-410.084240427393,-409.995812616232,
-409.907254480129,-409.883008743861,-409.794456591781,-409.706019196258,
-409.61767275306,-409.525875419976,-409.43763129807,-409.349400612134,-409.26116199341,
-409.172894072562,-409.084525771921,-408.99609796076,-408.907539824657,
-408.883294088388,-408.794741936308,-408.706304540785,-408.617958097587,
-408.526160764503,-408.437916642597,-408.349685956661,-408.261447337937,
-408.173179417088,-408.084811116446,-407.996383305285,-407.907825169182,
-407.883579432915,-407.795027280835,-407.706589885313,-407.618243442115,
-407.526446109031,-407.438201987125,-407.349971301189,-407.261732682465,
-407.173464761617,-407.085096460976,-406.996668649815,-406.908110513712,
-406.883864777443,-406.795383472727,-406.707014034475,-406.618734886537,
-406.530524528595,-406.442355489767,-406.354211255501,-406.266049699108,
-406.216608699687),.UNSPECIFIED.);
#414=B_SPLINE_CURVE_WITH_KNOTS('',3,(#63240,#63241,#63242,#63243,#63244,
#63245,#63246,#63247,#63248,#63249),.UNSPECIFIED.,.F.,.F.,(4,1,1,1,1,1,
1,4),(-406.216601437559,-405.88415012197,-404.884435466497,-403.884720811024,
-402.885006155551,-401.885291500078,-400.885576844606,-399.933423392507),
 .UNSPECIFIED.);
#415=B_SPLINE_CURVE_WITH_KNOTS('',3,(#63251,#63252,#63253,#63254,#63255,
#63256,#63257,#63258,#63259,#63260,#63261,#63262),.UNSPECIFIED.,.F.,.F.,
(4,2,1,1,1,1,1,1,4),(-399.933423392507,-399.885862189133,-398.88614753366,
-397.886432878187,-396.886718222714,-395.887003567241,-394.887288911769,
-393.887574256296,-393.650238085328),.UNSPECIFIED.);
#416=B_SPLINE_CURVE_WITH_KNOTS('',3,(#63264,#63265,#63266,#63267,#63268,
#63269,#63270,#63271,#63272,#63273),.UNSPECIFIED.,.F.,.F.,(4,1,1,1,1,1,
1,4),(-393.650238085328,-392.887859600823,-391.88814494535,-390.888430289877,
-389.888715634404,-388.889000978932,-387.889286323459,-387.367052778148),
 .UNSPECIFIED.);
#417=B_SPLINE_CURVE_WITH_KNOTS('',3,(#63275,#63276,#63277,#63278,#63279,
#63280,#63281,#63282,#63283,#63284),.UNSPECIFIED.,.F.,.F.,(4,1,1,1,1,1,
1,4),(-387.367052778148,-386.889571667986,-385.889857012513,-384.89014235704,
-383.890427701567,-382.890713046095,-381.890998390622,-381.083871454974),
 .UNSPECIFIED.);
#418=B_SPLINE_CURVE_WITH_KNOTS('',3,(#63286,#63287,#63288,#63289,#63290,
#63291,#63292,#63293,#63294,#63295,#63296,#63297,#63298,#63299,#63300,#63301,
#63302,#63303,#63304,#63305,#63306,#63307,#63308,#63309,#63310,#63311,#63312,
#63313,#63314,#63315,#63316,#63317,#63318,#63319,#63320,#63321,#63322,#63323,
#63324,#63325,#63326,#63327,#63328,#63329,#63330,#63331,#63332,#63333,#63334,
#63335,#63336,#63337,#63338,#63339,#63340,#63341,#63342,#63343,#63344,#63345,
#63346,#63347,#63348,#63349,#63350,#63351,#63352,#63353,#63354,#63355,#63356,
#63357,#63358,#63359,#63360,#63361,#63362,#63363,#63364,#63365,#63366,#63367,
#63368,#63369,#63370,#63371,#63372,#63373,#63374,#63375,#63376,#63377,#63378,
#63379,#63380,#63381,#63382,#63383,#63384,#63385,#63386,#63387,#63388,#63389,
#63390,#63391,#63392,#63393,#63394,#63395,#63396,#63397,#63398,#63399,#63400,
#63401,#63402,#63403,#63404,#63405,#63406,#63407,#63408,#63409,#63410,#63411,
#63412,#63413,#63414,#63415,#63416,#63417,#63418,#63419,#63420,#63421,#63422,
#63423,#63424,#63425,#63426,#63427,#63428,#63429,#63430,#63431,#63432,#63433,
#63434,#63435,#63436,#63437,#63438,#63439,#63440,#63441,#63442,#63443,#63444,
#63445,#63446,#63447,#63448,#63449,#63450,#63451,#63452,#63453,#63454,#63455,
#63456,#63457,#63458,#63459,#63460,#63461,#63462,#63463,#63464,#63465,#63466,
#63467,#63468,#63469,#63470,#63471,#63472,#63473,#63474,#63475,#63476,#63477,
#63478,#63479,#63480,#63481,#63482,#63483,#63484,#63485,#63486,#63487,#63488,
#63489,#63490,#63491,#63492,#63493,#63494,#63495,#63496,#63497,#63498,#63499,
#63500,#63501,#63502,#63503,#63504,#63505,#63506,#63507,#63508,#63509,#63510,
#63511),.UNSPECIFIED.,.F.,.F.,(4,3,3,3,3,3,3,3,3,3,3,3,3,3,3,3,3,3,3,3,
3,3,3,3,3,3,3,3,3,3,3,3,3,3,3,3,3,3,3,3,3,3,3,3,3,3,3,3,3,3,3,3,3,3,3,3,
3,3,3,3,3,3,3,3,3,3,3,3,3,3,3,3,3,3,3,4),(-381.083867470969,-380.954249617554,
-380.891283735149,-380.80273158307,-380.714294187547,-380.625947744349,
-380.534150411265,-380.445906289359,-380.357675603423,-380.2694369847,-380.181169063852,
-380.092800763211,-380.00437295205,-379.915814815947,-379.891569079676,
-379.803016927596,-379.714579532073,-379.626233088875,-379.534435755791,
-379.446191633885,-379.357960947949,-379.269722329225,-379.181454408376,
-379.093086107735,-379.004658296574,-378.916100160471,-378.891854424203,
-378.803302272123,-378.7148648766,-378.626518433402,-378.534721100318,-378.446476978411,
-378.358246292475,-378.270007673751,-378.181739752903,-378.093371452261,
-378.0049436411,-377.916385504997,-377.89213976873,-377.803587616651,-377.715150221128,
-377.62680377793,-377.535006444846,-377.44676232294,-377.358531637004,-377.27029301828,
-377.182025097432,-377.093656796791,-377.005228985631,-376.916670849528,
-376.892425113258,-376.803872961178,-376.715435565655,-376.627089122457,
-376.535291789373,-376.447047667467,-376.358816981531,-376.270578362807,
-376.182310441959,-376.093942141318,-376.005514330157,-375.916956194054,
-375.892710457785,-375.804158305705,-375.715720910182,-375.627374466984,
-375.5355771339,-375.447333011993,-375.359102326057,-375.270863707333,-375.182595786484,
-375.094227485843,-375.005799674682,-374.917241538579,-374.892995802312,
-374.800682163789),.UNSPECIFIED.);
#419=B_SPLINE_CURVE_WITH_KNOTS('',3,(#63513,#63514,#63515,#63516,#63517,
#63518,#63519,#63520,#63521,#63522),.UNSPECIFIED.,.F.,.F.,(4,1,1,1,1,1,
1,4),(-374.800673316255,-373.893281146839,-372.893566491366,-371.893851835893,
-370.894137180421,-369.894422524948,-368.894707869475,-368.517504463139),
 .UNSPECIFIED.);
#420=B_SPLINE_CURVE_WITH_KNOTS('',3,(#63524,#63525,#63526,#63527,#63528,
#63529,#63530,#63531,#63532,#63533,#63534,#63535,#63536,#63537,#63538,#63539,
#63540,#63541,#63542,#63543,#63544,#63545,#63546,#63547,#63548,#63549,#63550,
#63551,#63552,#63553,#63554,#63555,#63556,#63557,#63558,#63559,#63560,#63561,
#63562,#63563,#63564,#63565,#63566,#63567,#63568,#63569,#63570,#63571,#63572,
#63573,#63574,#63575,#63576,#63577,#63578,#63579,#63580,#63581,#63582,#63583,
#63584,#63585,#63586,#63587,#63588,#63589,#63590,#63591,#63592,#63593,#63594,
#63595,#63596,#63597,#63598,#63599,#63600,#63601,#63602,#63603,#63604,#63605,
#63606,#63607,#63608,#63609,#63610,#63611,#63612,#63613,#63614,#63615,#63616,
#63617,#63618,#63619,#63620,#63621,#63622,#63623,#63624,#63625,#63626,#63627,
#63628,#63629,#63630,#63631,#63632,#63633,#63634,#63635,#63636,#63637,#63638,
#63639,#63640,#63641,#63642,#63643,#63644,#63645,#63646,#63647,#63648,#63649,
#63650,#63651,#63652,#63653,#63654,#63655,#63656,#63657,#63658,#63659,#63660,
#63661,#63662,#63663,#63664,#63665,#63666,#63667,#63668,#63669,#63670,#63671,
#63672,#63673,#63674,#63675,#63676,#63677,#63678,#63679,#63680,#63681,#63682,
#63683,#63684,#63685,#63686,#63687,#63688,#63689,#63690,#63691,#63692,#63693,
#63694,#63695,#63696,#63697,#63698,#63699,#63700,#63701,#63702,#63703,#63704,
#63705,#63706,#63707,#63708,#63709,#63710,#63711,#63712,#63713,#63714,#63715,
#63716,#63717,#63718,#63719,#63720,#63721,#63722,#63723,#63724,#63725,#63726,
#63727,#63728,#63729,#63730,#63731,#63732,#63733,#63734,#63735,#63736,#63737,
#63738,#63739,#63740,#63741,#63742,#63743,#63744,#63745,#63746,#63747,#63748,
#63749),.UNSPECIFIED.,.F.,.F.,(4,3,3,3,3,3,3,3,3,3,3,3,3,3,3,3,3,3,3,3,
3,3,3,3,3,3,3,3,3,3,3,3,3,3,3,3,3,3,3,3,3,3,3,3,3,3,3,3,3,3,3,3,3,3,3,3,
3,3,3,3,3,3,3,3,3,3,3,3,3,3,3,3,3,3,3,4),(-368.517496856609,-368.428556137099,
-368.339605247134,-368.250623947272,-368.161527466105,-368.072373070321,
-367.983053193189,-367.894993214002,-367.806441061922,-367.718003666399,
-367.629657223201,-367.537859890117,-367.44961576821,-367.361385082274,
-367.27314646355,-367.184878542702,-367.09651024206,-367.008082430899,-366.919524294796,
-366.895278558529,-366.80672640645,-366.718289010927,-366.629942567729,
-366.538145234645,-366.449901112739,-366.361670426803,-366.273431808079,
-366.18516388723,-366.096795586589,-366.008367775429,-365.919809639326,
-365.895563903057,-365.807011750977,-365.718574355454,-365.630227912257,
-365.538430579173,-365.450186457267,-365.361955771331,-365.273717152607,
-365.185449231759,-365.097080931118,-365.008653119957,-364.920094983854,
-364.895849247584,-364.807297095504,-364.718859699981,-364.630513256783,
-364.538715923699,-364.450471801793,-364.362241115856,-364.274002497132,
-364.185734576284,-364.097366275643,-364.008938464481,-363.920380328378,
-363.896134592111,-363.807582440031,-363.719145044508,-363.630798601311,
-363.539001268226,-363.45075714632,-363.362526460384,-363.27428784166,-363.186019920812,
-363.09765162017,-363.009223809009,-362.920665672906,-362.896419936638,
-362.807853208516,-362.719399105434,-362.631036147201,-362.542742929627,
-362.454493271629,-362.366269341606,-362.278031497364,-362.23431154943),
 .UNSPECIFIED.);
#421=B_SPLINE_CURVE_WITH_KNOTS('',3,(#63751,#63752,#63753,#63754,#63755,
#63756,#63757,#63758,#63759,#63760),.UNSPECIFIED.,.F.,.F.,(4,1,1,1,1,1,
1,4),(-362.234304141519,-361.896705281165,-360.896990625692,-359.89727597022,
-358.897561314747,-357.897846659274,-356.898132003801,-355.95112624225),
 .UNSPECIFIED.);
#422=B_SPLINE_CURVE_WITH_KNOTS('',3,(#63762,#63763,#63764,#63765,#63766,
#63767,#63768,#63769,#63770,#63771,#63772,#63773),.UNSPECIFIED.,.F.,.F.,
(4,2,1,1,1,1,1,1,4),(-355.95112624225,-355.898417348328,-354.898702692855,
-353.898988037383,-352.89927338191,-351.899558726437,-350.899844070964,
-349.900129415491,-349.667940935071),.UNSPECIFIED.);
#423=B_SPLINE_CURVE_WITH_KNOTS('',3,(#63775,#63776,#63777,#63778,#63779,
#63780,#63781,#63782,#63783,#63784),.UNSPECIFIED.,.F.,.F.,(4,1,1,1,1,1,
1,4),(-349.667940935071,-348.900414760018,-347.900700104546,-346.900985449073,
-345.9012707936,-344.901556138127,-343.901841482654,-343.384755627891),
 .UNSPECIFIED.);
#424=B_SPLINE_CURVE_WITH_KNOTS('',3,(#63786,#63787,#63788,#63789,#63790,
#63791,#63792,#63793,#63794,#63795),.UNSPECIFIED.,.F.,.F.,(4,1,1,1,1,1,
1,4),(-343.384755627891,-342.902126827181,-341.902412171709,-340.902697516236,
-339.902982860763,-338.90326820529,-337.903553549817,-337.101573810142),
 .UNSPECIFIED.);
#425=B_SPLINE_CURVE_WITH_KNOTS('',3,(#63797,#63798,#63799,#63800,#63801,
#63802,#63803,#63804,#63805,#63806,#63807,#63808,#63809,#63810,#63811,#63812,
#63813,#63814,#63815,#63816,#63817,#63818,#63819,#63820,#63821,#63822,#63823,
#63824,#63825,#63826,#63827,#63828,#63829,#63830,#63831,#63832,#63833,#63834,
#63835,#63836,#63837,#63838,#63839,#63840,#63841,#63842,#63843,#63844,#63845,
#63846,#63847,#63848,#63849,#63850,#63851,#63852,#63853,#63854,#63855,#63856,
#63857,#63858,#63859,#63860,#63861,#63862,#63863,#63864,#63865,#63866,#63867,
#63868,#63869,#63870,#63871,#63872,#63873,#63874,#63875,#63876,#63877,#63878,
#63879,#63880,#63881,#63882,#63883,#63884,#63885,#63886,#63887,#63888,#63889,
#63890,#63891,#63892,#63893,#63894,#63895,#63896,#63897,#63898,#63899,#63900,
#63901,#63902,#63903,#63904,#63905,#63906,#63907,#63908,#63909,#63910,#63911,
#63912,#63913,#63914,#63915,#63916,#63917,#63918,#63919,#63920,#63921,#63922,
#63923,#63924,#63925,#63926,#63927,#63928,#63929,#63930,#63931,#63932,#63933,
#63934,#63935,#63936,#63937,#63938,#63939,#63940,#63941,#63942,#63943,#63944,
#63945,#63946,#63947,#63948,#63949,#63950,#63951,#63952,#63953,#63954,#63955,
#63956,#63957,#63958,#63959,#63960,#63961,#63962,#63963,#63964,#63965,#63966,
#63967,#63968,#63969,#63970,#63971,#63972,#63973,#63974,#63975,#63976,#63977,
#63978,#63979,#63980,#63981,#63982,#63983,#63984,#63985,#63986,#63987,#63988,
#63989,#63990,#63991,#63992,#63993,#63994,#63995,#63996,#63997,#63998,#63999,
#64000,#64001,#64002,#64003,#64004,#64005,#64006,#64007,#64008,#64009,#64010,
#64011,#64012,#64013,#64014,#64015,#64016,#64017,#64018,#64019,#64020,#64021,
#64022),.UNSPECIFIED.,.F.,.F.,(4,3,3,3,3,3,3,3,3,3,3,3,3,3,3,3,3,3,3,3,
3,3,3,3,3,3,3,3,3,3,3,3,3,3,3,3,3,3,3,3,3,3,3,3,3,3,3,3,3,3,3,3,3,3,3,3,
3,3,3,3,3,3,3,3,3,3,3,3,3,3,3,3,3,3,3,4),(-337.101570320712,-336.973722808615,
-336.903838894344,-336.815286742266,-336.726849346744,-336.638502903547,
-336.546705570463,-336.458461448558,-336.370230762624,-336.281992143901,
-336.193724223054,-336.105355922414,-336.016928111255,-335.928369975154,
-335.904124238872,-335.815572086792,-335.727134691269,-335.63878824807,
-335.546990914986,-335.45874679308,-335.370516107144,-335.28227748842,-335.194009567571,
-335.10564126693,-335.017213455768,-334.928655319665,-334.904409583399,
-334.815857431319,-334.727420035796,-334.639073592597,-334.547276259513,
-334.459032137607,-334.370801451671,-334.282562832946,-334.194294912098,
-334.105926611456,-334.017498800295,-333.928940664192,-333.904694927926,
-333.816142775847,-333.727705380324,-333.639358937126,-333.547561604042,
-333.459317482136,-333.3710867962,-333.282848177476,-333.194580256628,-333.106211955987,
-333.017784144826,-332.929226008723,-332.904980272453,-332.816428120373,
-332.72799072485,-332.639644281652,-332.547846948568,-332.459602826662,
-332.371372140726,-332.283133522002,-332.194865601153,-332.106497300512,
-332.018069489351,-331.929511353248,-331.90526561698,-331.8167134649,-331.728276069377,
-331.639929626179,-331.548132293095,-331.459888171189,-331.371657485253,
-331.283418866529,-331.19515094568,-331.106782645039,-331.018354833878,
-330.929796697775,-330.905550961507,-330.818385013532),.UNSPECIFIED.);
#426=B_SPLINE_CURVE_WITH_KNOTS('',3,(#64024,#64025,#64026,#64027,#64028,
#64029,#64030,#64031,#64032,#64033),.UNSPECIFIED.,.F.,.F.,(4,1,1,1,1,1,
1,4),(-330.818376289941,-329.905836306035,-328.906121650562,-327.906406995089,
-326.906692339616,-325.906977684143,-324.90726302867,-324.535207379122),
 .UNSPECIFIED.);
#427=B_SPLINE_CURVE_WITH_KNOTS('',3,(#64035,#64036,#64037,#64038,#64039,
#64040,#64041,#64042,#64043,#64044,#64045,#64046,#64047,#64048,#64049,#64050,
#64051,#64052,#64053,#64054,#64055,#64056,#64057,#64058,#64059,#64060,#64061,
#64062,#64063,#64064,#64065,#64066,#64067,#64068,#64069,#64070,#64071,#64072,
#64073,#64074,#64075,#64076,#64077,#64078,#64079,#64080,#64081,#64082,#64083,
#64084,#64085,#64086,#64087,#64088,#64089,#64090,#64091,#64092,#64093,#64094,
#64095,#64096,#64097,#64098,#64099,#64100,#64101,#64102,#64103,#64104,#64105,
#64106,#64107,#64108,#64109,#64110,#64111,#64112,#64113,#64114,#64115,#64116,
#64117,#64118,#64119,#64120,#64121,#64122,#64123,#64124,#64125,#64126,#64127,
#64128,#64129,#64130,#64131,#64132,#64133,#64134,#64135,#64136,#64137,#64138,
#64139,#64140,#64141,#64142,#64143,#64144,#64145,#64146,#64147,#64148,#64149,
#64150,#64151,#64152,#64153,#64154,#64155,#64156,#64157,#64158,#64159,#64160,
#64161,#64162,#64163,#64164,#64165,#64166,#64167,#64168,#64169,#64170,#64171,
#64172,#64173,#64174,#64175,#64176,#64177,#64178,#64179,#64180,#64181,#64182,
#64183,#64184,#64185,#64186,#64187,#64188,#64189,#64190,#64191,#64192,#64193,
#64194,#64195,#64196,#64197,#64198,#64199,#64200,#64201,#64202,#64203,#64204,
#64205,#64206,#64207,#64208,#64209,#64210,#64211,#64212,#64213,#64214,#64215,
#64216,#64217,#64218,#64219,#64220,#64221,#64222,#64223,#64224,#64225,#64226,
#64227,#64228,#64229,#64230,#64231,#64232,#64233,#64234,#64235,#64236,#64237,
#64238,#64239,#64240,#64241,#64242,#64243,#64244,#64245,#64246,#64247,#64248,
#64249,#64250,#64251,#64252,#64253,#64254,#64255,#64256,#64257,#64258,#64259,
#64260),.UNSPECIFIED.,.F.,.F.,(4,3,3,3,3,3,3,3,3,3,3,3,3,3,3,3,3,3,3,3,
3,3,3,3,3,3,3,3,3,3,3,3,3,3,3,3,3,3,3,3,3,3,3,3,3,3,3,3,3,3,3,3,3,3,3,3,
3,3,3,3,3,3,3,3,3,3,3,3,3,3,3,3,3,3,3,4),(-324.535199706353,-324.446359815449,
-324.357512939538,-324.268638672611,-324.178366097758,-324.089322870752,
-323.998435621975,-323.907548373198,-323.818996221118,-323.730558825595,
-323.642212382397,-323.550415049313,-323.462170927407,-323.373940241471,
-323.285701622747,-323.197433701898,-323.109065401257,-323.020637590096,
-322.932079453993,-322.907833717725,-322.819281565645,-322.730844170122,
-322.642497726924,-322.55070039384,-322.462456271934,-322.374225585998,
-322.285986967274,-322.197719046425,-322.109350745784,-322.020922934623,
-321.93236479852,-321.908119062252,-321.819566910172,-321.731129514649,
-321.642783071451,-321.550985738367,-321.462741616461,-321.374510930525,
-321.286272311801,-321.198004390953,-321.109636090311,-321.021208279151,
-320.932650143048,-320.908404406779,-320.819852254699,-320.731414859176,
-320.643068415978,-320.551271082894,-320.463026960988,-320.374796275052,
-320.286557656327,-320.198289735479,-320.109921434838,-320.021493623676,
-319.932935487573,-319.908689751306,-319.820137599226,-319.731700203703,
-319.643353760505,-319.551556427421,-319.463312305515,-319.375081619579,
-319.286843000855,-319.198575080007,-319.110206779366,-319.021778968205,
-318.933220832102,-318.908975095833,-318.82031988714,-318.73177809888,-318.643328353439,
-318.554949349457,-318.46661619347,-318.37830974425,-318.289992754975,-318.252014399173),
 .UNSPECIFIED.);
#428=B_SPLINE_CURVE_WITH_KNOTS('',3,(#64262,#64263,#64264,#64265,#64266,
#64267,#64268,#64269,#64270,#64271,#64272,#64273,#64274,#64275,#64276,#64277,
#64278,#64279,#64280,#64281,#64282,#64283,#64284,#64285,#64286,#64287,#64288,
#64289,#64290,#64291,#64292,#64293,#64294,#64295,#64296,#64297,#64298,#64299,
#64300,#64301,#64302,#64303,#64304,#64305,#64306,#64307,#64308,#64309,#64310,
#64311,#64312,#64313,#64314,#64315,#64316,#64317,#64318,#64319,#64320,#64321,
#64322,#64323,#64324,#64325,#64326,#64327,#64328,#64329,#64330,#64331,#64332,
#64333,#64334,#64335,#64336,#64337,#64338,#64339,#64340,#64341,#64342,#64343,
#64344,#64345,#64346,#64347,#64348,#64349,#64350,#64351,#64352,#64353,#64354,
#64355,#64356,#64357,#64358,#64359,#64360,#64361,#64362,#64363,#64364,#64365,
#64366,#64367,#64368,#64369,#64370,#64371,#64372,#64373,#64374,#64375,#64376,
#64377,#64378,#64379,#64380,#64381,#64382,#64383,#64384,#64385,#64386,#64387,
#64388,#64389,#64390,#64391,#64392,#64393,#64394,#64395,#64396,#64397,#64398,
#64399,#64400,#64401,#64402,#64403,#64404,#64405,#64406,#64407,#64408,#64409,
#64410,#64411,#64412,#64413,#64414,#64415,#64416,#64417,#64418,#64419,#64420,
#64421,#64422,#64423,#64424,#64425,#64426,#64427,#64428,#64429,#64430,#64431,
#64432,#64433,#64434,#64435,#64436,#64437,#64438,#64439,#64440,#64441,#64442,
#64443,#64444,#64445,#64446,#64447,#64448,#64449,#64450,#64451,#64452,#64453,
#64454,#64455,#64456,#64457,#64458,#64459,#64460,#64461,#64462,#64463,#64464,
#64465,#64466,#64467,#64468,#64469,#64470,#64471,#64472,#64473,#64474,#64475,
#64476,#64477,#64478,#64479,#64480,#64481,#64482,#64483,#64484,#64485,#64486,
#64487),.UNSPECIFIED.,.F.,.F.,(4,3,3,3,3,3,3,3,3,3,3,3,3,3,3,3,3,3,3,3,
3,3,3,3,3,3,3,3,3,3,3,3,3,3,3,3,3,3,3,3,3,3,3,3,3,3,3,3,3,3,3,3,3,3,3,3,
3,3,3,3,3,3,3,3,3,3,3,3,3,3,3,3,3,3,3,4),(-318.252014398944,-318.150053608736,
-318.04751572947,-317.944304068901,-317.909260440361,-317.820708288281,
-317.732270892758,-317.643924449559,-317.552127116475,-317.463882994569,
-317.375652308632,-317.287413689908,-317.19914576906,-317.110777468418,
-317.022349657257,-316.933791521154,-316.909545784888,-316.820993632808,
-316.732556237285,-316.644209794087,-316.552412461003,-316.464168339097,
-316.375937653161,-316.287699034437,-316.199431113589,-316.111062812948,
-316.022635001787,-315.934076865684,-315.909831129415,-315.821278977335,
-315.732841581812,-315.644495138614,-315.55269780553,-315.464453683624,
-315.376222997688,-315.287984378964,-315.199716458116,-315.111348157475,
-315.022920346314,-314.934362210211,-314.910116473942,-314.821564321862,
-314.733126926339,-314.644780483141,-314.552983150057,-314.464739028151,
-314.376508342215,-314.288269723491,-314.200001802642,-314.111633502001,
-314.02320569084,-313.934647554737,-313.910401818469,-313.821849666389,
-313.733412270866,-313.645065827668,-313.553268494584,-313.465024372678,
-313.376793686742,-313.288555068018,-313.200287147169,-313.111918846528,
-313.023491035367,-312.934932899264,-312.910687162996,-312.822895988953,
-312.73521894255,-312.647631400734,-312.560107192341,-312.472615981098,
-312.3851356625,-312.297644145287,-312.210067236098,-312.12244558037,-312.034688551243,
-311.968829091993),.UNSPECIFIED.);
#429=B_SPLINE_CURVE_WITH_KNOTS('',3,(#64489,#64490,#64491,#64492,#64493,
#64494,#64495,#64496,#64497,#64498,#64499,#64500),.UNSPECIFIED.,.F.,.F.,
(4,2,1,1,1,1,1,1,4),(-311.968829091993,-311.910972507524,-310.911257852051,
-309.911543196578,-308.911828541105,-307.912113885632,-306.912399230159,
-305.912684574687,-305.685643784814),.UNSPECIFIED.);
#430=B_SPLINE_CURVE_WITH_KNOTS('',3,(#64502,#64503,#64504,#64505,#64506,
#64507,#64508,#64509,#64510,#64511,#64512,#64513,#64514,#64515,#64516,#64517,
#64518,#64519,#64520,#64521,#64522,#64523,#64524,#64525,#64526,#64527,#64528,
#64529,#64530,#64531,#64532,#64533,#64534,#64535,#64536,#64537,#64538,#64539,
#64540,#64541,#64542,#64543,#64544,#64545,#64546,#64547,#64548,#64549,#64550,
#64551,#64552,#64553,#64554,#64555,#64556,#64557,#64558,#64559,#64560,#64561,
#64562,#64563,#64564,#64565,#64566,#64567,#64568,#64569,#64570,#64571,#64572,
#64573,#64574,#64575,#64576,#64577,#64578,#64579,#64580,#64581,#64582,#64583,
#64584,#64585,#64586,#64587,#64588,#64589,#64590,#64591,#64592,#64593,#64594,
#64595,#64596,#64597,#64598,#64599,#64600,#64601,#64602,#64603,#64604,#64605,
#64606,#64607,#64608,#64609,#64610,#64611,#64612,#64613,#64614,#64615,#64616,
#64617,#64618,#64619,#64620,#64621,#64622,#64623,#64624,#64625,#64626,#64627,
#64628,#64629,#64630,#64631,#64632,#64633,#64634,#64635,#64636,#64637,#64638,
#64639,#64640,#64641,#64642,#64643,#64644,#64645,#64646,#64647,#64648,#64649,
#64650,#64651,#64652,#64653,#64654,#64655,#64656,#64657,#64658,#64659,#64660,
#64661,#64662,#64663,#64664,#64665,#64666,#64667,#64668,#64669,#64670,#64671,
#64672,#64673,#64674,#64675,#64676,#64677,#64678,#64679,#64680,#64681,#64682,
#64683,#64684,#64685,#64686,#64687,#64688,#64689,#64690,#64691,#64692,#64693,
#64694,#64695,#64696,#64697,#64698,#64699,#64700,#64701,#64702,#64703,#64704,
#64705,#64706,#64707,#64708,#64709,#64710,#64711,#64712,#64713,#64714,#64715,
#64716,#64717,#64718,#64719,#64720,#64721,#64722,#64723,#64724,#64725,#64726,
#64727),.UNSPECIFIED.,.F.,.F.,(4,3,3,3,3,3,3,3,3,3,3,3,3,3,3,3,3,3,3,3,
3,3,3,3,3,3,3,3,3,3,3,3,3,3,3,3,3,3,3,3,3,3,3,3,3,3,3,3,3,3,3,3,3,3,3,3,
3,3,3,3,3,3,3,3,3,3,3,3,3,3,3,3,3,3,3,4),(-305.685643784814,-305.598454037272,
-305.511330089946,-305.424240779258,-305.337163689709,-305.250076420172,
-305.162901898749,-305.075683108739,-304.988322318422,-304.912969919214,
-304.824417767134,-304.735980371611,-304.647633928413,-304.555836595329,
-304.467592473423,-304.379361787487,-304.291123168763,-304.202855247914,
-304.114486947273,-304.026059136112,-303.937501000009,-303.913255263741,
-303.824703111661,-303.736265716138,-303.64791927294,-303.556121939856,
-303.46787781795,-303.379647132014,-303.29140851329,-303.203140592442,-303.114772291801,
-303.02634448064,-302.937786344537,-302.913540608268,-302.824988456188,
-302.736551060665,-302.648204617467,-302.556407284383,-302.468163162477,
-302.379932476541,-302.291693857817,-302.203425936968,-302.115057636327,
-302.026629825166,-301.938071689063,-301.913825952795,-301.825273800715,
-301.736836405192,-301.648489961994,-301.55669262891,-301.468448507004,
-301.380217821067,-301.291979202343,-301.203711281495,-301.115342980854,
-301.026915169693,-300.93835703359,-300.914111297322,-300.825559145243,
-300.73712174972,-300.648775306523,-300.556977973439,-300.468733851533,
-300.380503165597,-300.292264546873,-300.203996626025,-300.115628325384,
-300.027200514223,-299.938642378121,-299.91439664185,-299.821768244774,
-299.72930162526,-299.637039091217,-299.54489838375,-299.45290684345,-299.402458477634),
 .UNSPECIFIED.);
#431=B_SPLINE_CURVE_WITH_KNOTS('',3,(#64729,#64730,#64731,#64732,#64733,
#64734,#64735,#64736,#64737,#64738,#64739,#64740,#64741,#64742,#64743,#64744,
#64745,#64746,#64747,#64748,#64749,#64750,#64751,#64752,#64753,#64754,#64755,
#64756,#64757,#64758,#64759,#64760,#64761,#64762,#64763,#64764,#64765,#64766,
#64767,#64768,#64769,#64770,#64771,#64772,#64773,#64774,#64775,#64776,#64777,
#64778,#64779,#64780,#64781,#64782,#64783,#64784,#64785,#64786,#64787,#64788,
#64789,#64790,#64791,#64792,#64793,#64794,#64795,#64796,#64797,#64798,#64799,
#64800,#64801,#64802,#64803,#64804,#64805,#64806,#64807,#64808,#64809,#64810,
#64811,#64812,#64813,#64814,#64815,#64816,#64817,#64818,#64819,#64820,#64821,
#64822,#64823,#64824,#64825,#64826,#64827,#64828,#64829,#64830,#64831,#64832,
#64833,#64834,#64835,#64836,#64837,#64838,#64839,#64840,#64841,#64842,#64843,
#64844,#64845,#64846,#64847,#64848,#64849,#64850,#64851,#64852,#64853,#64854,
#64855,#64856,#64857,#64858,#64859,#64860,#64861,#64862,#64863,#64864,#64865,
#64866,#64867,#64868,#64869,#64870,#64871,#64872,#64873,#64874,#64875,#64876,
#64877,#64878,#64879,#64880,#64881,#64882,#64883,#64884,#64885,#64886,#64887,
#64888,#64889,#64890,#64891,#64892,#64893,#64894,#64895,#64896,#64897,#64898,
#64899,#64900,#64901,#64902,#64903,#64904,#64905,#64906,#64907,#64908,#64909,
#64910,#64911,#64912,#64913,#64914,#64915,#64916,#64917,#64918,#64919,#64920,
#64921,#64922,#64923,#64924,#64925,#64926,#64927,#64928,#64929,#64930,#64931,
#64932,#64933,#64934,#64935,#64936,#64937,#64938,#64939,#64940,#64941,#64942,
#64943,#64944,#64945,#64946,#64947,#64948,#64949,#64950,#64951,#64952,#64953,
#64954),.UNSPECIFIED.,.F.,.F.,(4,3,3,3,3,3,3,3,3,3,3,3,3,3,3,3,3,3,3,3,
3,3,3,3,3,3,3,3,3,3,3,3,3,3,3,3,3,3,3,3,3,3,3,3,3,3,3,3,3,3,3,3,3,3,3,3,
3,3,3,3,3,3,3,3,3,3,3,3,3,3,3,3,3,3,3,4),(-299.402458477502,-299.309553527439,
-299.216500663027,-299.123205464595,-299.029774917432,-298.936131896398,
-298.914681986377,-298.826129834297,-298.737692438774,-298.649345995575,
-298.557548662491,-298.469304540585,-298.381073854649,-298.292835235925,
-298.204567315076,-298.116199014434,-298.027771203273,-297.93921306717,
-297.914967330904,-297.826415178824,-297.737977783301,-297.649631340103,
-297.557834007019,-297.469589885113,-297.381359199177,-297.293120580453,
-297.204852659604,-297.116484358963,-297.028056547802,-296.939498411699,
-296.915252675431,-296.826700523351,-296.738263127828,-296.64991668463,
-296.558119351546,-296.46987522964,-296.381644543704,-296.29340592498,-296.205138004132,
-296.116769703491,-296.02834189233,-295.939783756227,-295.915538019958,
-295.826985867878,-295.738548472355,-295.650202029157,-295.558404696073,
-295.470160574166,-295.38192988823,-295.293691269506,-295.205423348658,
-295.117055048016,-295.028627236855,-294.940069100752,-294.915823364485,
-294.827271212406,-294.738833816883,-294.650487373685,-294.558690040601,
-294.470445918695,-294.382215232759,-294.293976614035,-294.205708693187,
-294.117340392546,-294.028912581385,-293.940354445283,-293.916108709013,
-293.828823892562,-293.740130052298,-293.65306297726,-293.566051538638,
-293.479073216952,-293.389123205328,-293.30211266917,-293.210692919813,
-293.119273170455),.UNSPECIFIED.);
#432=B_SPLINE_CURVE_WITH_KNOTS('',3,(#64956,#64957,#64958,#64959,#64960,
#64961,#64962,#64963,#64964,#64965,#64966),.UNSPECIFIED.,.F.,.F.,(4,1,1,
1,1,1,1,1,4),(-293.119273170455,-292.91639405354,-291.916679398067,-290.916964742594,
-289.917250087121,-288.917535431648,-287.917820776176,-286.918106120703,
-286.836087863275),.UNSPECIFIED.);
#433=B_SPLINE_CURVE_WITH_KNOTS('',3,(#64968,#64969,#64970,#64971,#64972,
#64973,#64974,#64975,#64976,#64977),.UNSPECIFIED.,.F.,.F.,(4,1,1,1,1,1,
1,4),(-286.836087863275,-285.91839146523,-284.918676809757,-283.918962154284,
-282.919247498811,-281.919532843339,-280.919818187866,-280.552902556096),
 .UNSPECIFIED.);
#434=B_SPLINE_CURVE_WITH_KNOTS('',3,(#64979,#64980,#64981,#64982,#64983,
#64984,#64985,#64986,#64987,#64988),.UNSPECIFIED.,.F.,.F.,(4,1,1,1,1,1,
1,4),(-280.552902556096,-279.920103532393,-278.92038887692,-277.920674221447,
-276.920959565974,-275.921244910502,-274.921530255029,-274.269717248916),
 .UNSPECIFIED.);
#435=B_SPLINE_CURVE_WITH_KNOTS('',3,(#64990,#64991,#64992,#64993,#64994,
#64995,#64996,#64997,#64998,#64999,#65000,#65001,#65002,#65003,#65004,#65005,
#65006,#65007,#65008,#65009,#65010,#65011,#65012,#65013,#65014,#65015,#65016,
#65017,#65018,#65019,#65020,#65021,#65022,#65023,#65024,#65025,#65026,#65027,
#65028,#65029,#65030,#65031,#65032,#65033,#65034,#65035,#65036,#65037,#65038,
#65039,#65040,#65041,#65042,#65043,#65044,#65045,#65046,#65047,#65048,#65049,
#65050,#65051,#65052,#65053,#65054,#65055,#65056,#65057,#65058,#65059,#65060,
#65061,#65062,#65063,#65064,#65065,#65066,#65067,#65068,#65069,#65070,#65071,
#65072,#65073,#65074,#65075,#65076,#65077,#65078,#65079,#65080,#65081,#65082,
#65083,#65084,#65085,#65086,#65087,#65088,#65089,#65090,#65091,#65092,#65093,
#65094,#65095,#65096,#65097,#65098,#65099,#65100,#65101,#65102,#65103,#65104,
#65105,#65106,#65107,#65108,#65109,#65110,#65111,#65112,#65113,#65114,#65115,
#65116,#65117,#65118,#65119,#65120,#65121,#65122,#65123,#65124,#65125,#65126,
#65127,#65128,#65129,#65130,#65131,#65132,#65133,#65134,#65135,#65136,#65137,
#65138,#65139,#65140,#65141,#65142,#65143,#65144,#65145,#65146,#65147,#65148,
#65149,#65150,#65151,#65152,#65153,#65154,#65155,#65156,#65157,#65158,#65159,
#65160,#65161,#65162,#65163,#65164,#65165,#65166,#65167,#65168,#65169,#65170,
#65171,#65172,#65173,#65174,#65175,#65176,#65177,#65178,#65179,#65180,#65181,
#65182,#65183,#65184,#65185,#65186,#65187,#65188,#65189,#65190,#65191,#65192,
#65193,#65194,#65195,#65196,#65197,#65198,#65199,#65200,#65201,#65202,#65203,
#65204,#65205,#65206,#65207,#65208,#65209,#65210,#65211,#65212,#65213,#65214,
#65215),.UNSPECIFIED.,.F.,.F.,(4,3,3,3,3,3,3,3,3,3,3,3,3,3,3,3,3,3,3,3,
3,3,3,3,3,3,3,3,3,3,3,3,3,3,3,3,3,3,3,3,3,3,3,3,3,3,3,3,3,3,3,3,3,3,3,3,
3,3,3,3,3,3,3,3,3,3,3,3,3,3,3,3,3,3,3,4),(-274.269717004602,-274.168208143946,
-274.066155437434,-273.963451878141,-273.921815599556,-273.833263447476,
-273.744826051953,-273.656479608755,-273.564682275671,-273.476438153764,
-273.388207467828,-273.299968849104,-273.211700928256,-273.123332627614,
-273.034904816453,-272.94634668035,-272.922100944083,-272.833548792003,
-272.74511139648,-272.656764953282,-272.564967620198,-272.476723498292,
-272.388492812356,-272.300254193632,-272.211986272784,-272.123617972142,
-272.035190160981,-271.946632024879,-271.92238628861,-271.83383413653,-271.745396741007,
-271.657050297809,-271.565252964725,-271.477008842819,-271.388778156882,
-271.300539538159,-271.21227161731,-271.123903316669,-271.035475505508,
-270.946917369405,-270.922671633137,-270.834119481058,-270.745682085535,
-270.657335642337,-270.565538309253,-270.477294187347,-270.389063501411,
-270.300824882687,-270.212556961839,-270.124188661198,-270.035760850037,
-269.947202713935,-269.922956977665,-269.834404825585,-269.745967430062,
-269.657620986864,-269.56582365378,-269.477579531874,-269.389348845938,
-269.301110227215,-269.212842306366,-269.124474005725,-269.036046194564,
-268.947488058461,-268.923242322192,-268.835502740503,-268.747877234083,
-268.660341131574,-268.572868278738,-268.485428267421,-268.397998951407,
-268.310558197594,-268.223032677745,-268.135462093365,-268.047758426598,
-267.986531941736),.UNSPECIFIED.);
#436=B_SPLINE_CURVE_WITH_KNOTS('',3,(#65217,#65218,#65219,#65220,#65221,
#65222,#65223,#65224,#65225,#65226,#65227,#65228),.UNSPECIFIED.,.F.,.F.,
(4,2,1,1,1,1,1,1,4),(-267.986531941736,-267.923527666719,-266.923813011246,
-265.924098355773,-264.9243837003,-263.924669044828,-262.924954389355,-261.925239733882,
-261.703346634557),.UNSPECIFIED.);
#437=B_SPLINE_CURVE_WITH_KNOTS('',3,(#65230,#65231,#65232,#65233,#65234,
#65235,#65236,#65237,#65238,#65239,#65240,#65241,#65242,#65243,#65244,#65245,
#65246,#65247,#65248,#65249,#65250,#65251,#65252,#65253,#65254,#65255,#65256,
#65257,#65258,#65259,#65260,#65261,#65262,#65263,#65264,#65265,#65266,#65267,
#65268,#65269,#65270,#65271,#65272,#65273,#65274,#65275,#65276,#65277,#65278,
#65279,#65280,#65281,#65282,#65283,#65284,#65285,#65286,#65287,#65288,#65289,
#65290,#65291,#65292,#65293,#65294,#65295,#65296,#65297,#65298,#65299,#65300,
#65301,#65302,#65303,#65304,#65305,#65306,#65307,#65308,#65309,#65310,#65311,
#65312,#65313,#65314,#65315,#65316,#65317,#65318,#65319,#65320,#65321,#65322,
#65323,#65324,#65325,#65326,#65327,#65328,#65329,#65330,#65331,#65332,#65333,
#65334,#65335,#65336,#65337,#65338,#65339,#65340,#65341,#65342,#65343,#65344,
#65345,#65346,#65347,#65348,#65349,#65350,#65351,#65352,#65353,#65354,#65355,
#65356,#65357,#65358,#65359,#65360,#65361,#65362,#65363,#65364,#65365,#65366,
#65367,#65368,#65369,#65370,#65371,#65372,#65373,#65374,#65375,#65376,#65377,
#65378,#65379,#65380,#65381,#65382,#65383,#65384,#65385,#65386,#65387,#65388,
#65389,#65390,#65391,#65392,#65393,#65394,#65395,#65396,#65397,#65398,#65399,
#65400,#65401,#65402,#65403,#65404,#65405,#65406,#65407,#65408,#65409,#65410,
#65411,#65412,#65413,#65414,#65415,#65416,#65417,#65418,#65419,#65420,#65421,
#65422,#65423,#65424,#65425,#65426,#65427,#65428,#65429,#65430,#65431,#65432,
#65433,#65434,#65435,#65436,#65437,#65438,#65439,#65440,#65441,#65442,#65443,
#65444,#65445,#65446,#65447,#65448,#65449,#65450,#65451,#65452,#65453,#65454,
#65455),.UNSPECIFIED.,.F.,.F.,(4,3,3,3,3,3,3,3,3,3,3,3,3,3,3,3,3,3,3,3,
3,3,3,3,3,3,3,3,3,3,3,3,3,3,3,3,3,3,3,3,3,3,3,3,3,3,3,3,3,3,3,3,3,3,3,3,
3,3,3,3,3,3,3,3,3,3,3,3,3,3,3,3,3,3,3,4),(-261.703346634557,-261.616176758673,
-261.529075180752,-261.442009868448,-261.35495838563,-261.267898311999,
-261.180752041239,-261.093562892726,-261.006230334554,-260.925525078409,
-260.836972926329,-260.748535530806,-260.660189087608,-260.568391754524,
-260.480147632618,-260.391916946682,-260.303678327958,-260.21541040711,
-260.127042106468,-260.038614295307,-259.950056159204,-259.925810422936,
-259.837258270856,-259.748820875333,-259.660474432135,-259.568677099051,
-259.480432977145,-259.392202291209,-259.303963672485,-259.215695751636,
-259.127327450994,-259.038899639833,-258.95034150373,-258.926095767463,
-258.837543615383,-258.749106219861,-258.660759776663,-258.568962443579,
-258.480718321673,-258.392487635737,-258.304249017013,-258.215981096165,
-258.127612795524,-258.039184984363,-257.950626848261,-257.926381111991,
-257.837828959912,-257.749391564388,-257.66104512119,-257.569247788106,
-257.4810036662,-257.392772980264,-257.30453436154,-257.216266440692,-257.127898140051,
-257.03947032889,-256.950912192787,-256.926666456518,-256.838114304438,
-256.749676908915,-256.661330465717,-256.569533132633,-256.481289010727,
-256.393058324791,-256.304819706067,-256.216551785218,-256.128183484577,
-256.039755673416,-255.951197537313,-255.926951801045,-255.834118795862,
-255.741450830476,-255.648992944735,-255.556661144641,-255.46448525518,
-255.420161327377),.UNSPECIFIED.);
#438=B_SPLINE_CURVE_WITH_KNOTS('',3,(#65457,#65458,#65459,#65460,#65461,
#65462,#65463,#65464,#65465,#65466,#65467,#65468,#65469,#65470,#65471,#65472,
#65473,#65474,#65475,#65476,#65477,#65478,#65479,#65480,#65481,#65482,#65483,
#65484,#65485,#65486,#65487,#65488,#65489,#65490,#65491,#65492,#65493,#65494,
#65495,#65496,#65497,#65498,#65499,#65500,#65501,#65502,#65503,#65504,#65505,
#65506,#65507,#65508,#65509,#65510,#65511,#65512,#65513,#65514,#65515,#65516,
#65517,#65518,#65519,#65520,#65521,#65522,#65523,#65524,#65525,#65526,#65527,
#65528,#65529,#65530,#65531,#65532,#65533,#65534,#65535,#65536,#65537,#65538,
#65539,#65540,#65541,#65542,#65543,#65544,#65545,#65546,#65547,#65548,#65549,
#65550,#65551,#65552,#65553,#65554,#65555,#65556,#65557,#65558,#65559,#65560,
#65561,#65562,#65563,#65564,#65565,#65566,#65567,#65568,#65569,#65570,#65571,
#65572,#65573,#65574,#65575,#65576,#65577,#65578,#65579,#65580,#65581,#65582,
#65583,#65584,#65585,#65586,#65587,#65588,#65589,#65590,#65591,#65592,#65593,
#65594,#65595,#65596,#65597,#65598,#65599,#65600,#65601,#65602,#65603,#65604,
#65605,#65606,#65607,#65608,#65609,#65610,#65611,#65612,#65613,#65614,#65615,
#65616,#65617,#65618,#65619,#65620,#65621,#65622,#65623,#65624,#65625,#65626,
#65627,#65628,#65629,#65630,#65631,#65632,#65633,#65634,#65635,#65636,#65637,
#65638,#65639,#65640,#65641,#65642,#65643,#65644,#65645,#65646,#65647,#65648,
#65649,#65650,#65651,#65652,#65653,#65654,#65655,#65656,#65657,#65658,#65659,
#65660,#65661,#65662,#65663,#65664,#65665,#65666,#65667,#65668,#65669,#65670,
#65671,#65672,#65673,#65674,#65675,#65676,#65677,#65678,#65679,#65680,#65681,
#65682),.UNSPECIFIED.,.F.,.F.,(4,3,3,3,3,3,3,3,3,3,3,3,3,3,3,3,3,3,3,3,
3,3,3,3,3,3,3,3,3,3,3,3,3,3,3,3,3,3,3,3,3,3,3,3,3,3,3,3,3,3,3,3,3,3,3,3,
3,3,3,3,3,3,3,3,3,3,3,3,3,3,3,3,3,3,3,4),(-255.420161327226,-255.327463107471,
-255.234625308542,-255.141553107975,-255.048350781773,-254.954937477772,
-254.927237145572,-254.838684993492,-254.750247597969,-254.661901154771,
-254.570103821687,-254.48185969978,-254.393629013844,-254.30539039512,-254.217122474272,
-254.12875417363,-254.040326362469,-253.951768226366,-253.927522490099,
-253.838970338019,-253.750532942496,-253.662186499298,-253.570389166214,
-253.482145044308,-253.393914358371,-253.305675739647,-253.217407818799,
-253.129039518158,-253.040611706997,-252.952053570894,-252.927807834626,
-252.839255682547,-252.750818287024,-252.662471843826,-252.570674510742,
-252.482430388836,-252.3941997029,-252.305961084176,-252.217693163328,-252.129324862687,
-252.040897051527,-251.952338915424,-251.928093179154,-251.839541027074,
-251.751103631551,-251.662757188353,-251.570959855269,-251.482715733363,
-251.394485047427,-251.306246428703,-251.217978507855,-251.129610207213,
-251.041182396052,-250.95262425995,-250.928378523681,-250.839826371601,
-250.751388976078,-250.66304253288,-250.571245199796,-250.483001077889,
-250.394770391953,-250.306531773229,-250.218263852381,-250.129895551739,
-250.041467740578,-249.952909604475,-249.928663868208,-249.841361323148,
-249.753313160279,-249.666228402379,-249.579199673663,-249.492204465771,
-249.403397354378,-249.316372070933,-249.226674045566,-249.136976020198),
 .UNSPECIFIED.);
#439=B_SPLINE_CURVE_WITH_KNOTS('',3,(#65684,#65685,#65686,#65687,#65688,
#65689,#65690,#65691,#65692,#65693,#65694),.UNSPECIFIED.,.F.,.F.,(4,1,1,
1,1,1,1,1,4),(-249.136976020198,-248.928949212735,-247.929234557262,-246.92951990179,
-245.929805246317,-244.930090590844,-243.930375935371,-242.930661279898,
-242.853790713018),.UNSPECIFIED.);
#440=B_SPLINE_CURVE_WITH_KNOTS('',3,(#65696,#65697,#65698,#65699,#65700,
#65701,#65702,#65703,#65704,#65705),.UNSPECIFIED.,.F.,.F.,(4,1,1,1,1,1,
1,4),(-242.853790713018,-241.930946624425,-240.931231968953,-239.93151731348,
-238.931802658007,-237.932088002534,-236.932373347061,-236.570605405839),
 .UNSPECIFIED.);
#441=B_SPLINE_CURVE_WITH_KNOTS('',3,(#65707,#65708,#65709,#65710,#65711,
#65712,#65713,#65714,#65715,#65716),.UNSPECIFIED.,.F.,.F.,(4,1,1,1,1,1,
1,4),(-236.570605405839,-235.932658691588,-234.932944036115,-233.933229380643,
-232.93351472517,-231.933800069697,-230.934085414224,-230.287420098659),
 .UNSPECIFIED.);
#442=B_SPLINE_CURVE_WITH_KNOTS('',3,(#65718,#65719,#65720,#65721,#65722,
#65723,#65724,#65725,#65726,#65727,#65728,#65729,#65730,#65731,#65732,#65733,
#65734,#65735,#65736,#65737,#65738,#65739,#65740,#65741,#65742,#65743,#65744,
#65745,#65746,#65747,#65748,#65749,#65750,#65751,#65752,#65753,#65754,#65755,
#65756,#65757,#65758,#65759,#65760,#65761,#65762,#65763,#65764,#65765,#65766,
#65767,#65768,#65769,#65770,#65771,#65772,#65773,#65774,#65775,#65776,#65777,
#65778,#65779,#65780,#65781,#65782,#65783,#65784,#65785,#65786,#65787,#65788,
#65789,#65790,#65791,#65792,#65793,#65794,#65795,#65796,#65797,#65798,#65799,
#65800,#65801,#65802,#65803,#65804,#65805,#65806,#65807,#65808,#65809,#65810,
#65811,#65812,#65813,#65814,#65815,#65816,#65817,#65818,#65819,#65820,#65821,
#65822,#65823,#65824,#65825,#65826,#65827,#65828,#65829,#65830,#65831,#65832,
#65833,#65834,#65835,#65836,#65837,#65838,#65839,#65840,#65841,#65842,#65843,
#65844,#65845,#65846,#65847,#65848,#65849,#65850,#65851,#65852,#65853,#65854,
#65855,#65856,#65857,#65858,#65859,#65860,#65861,#65862,#65863,#65864,#65865,
#65866,#65867,#65868,#65869,#65870,#65871,#65872,#65873,#65874,#65875,#65876,
#65877,#65878,#65879,#65880,#65881,#65882,#65883,#65884,#65885,#65886,#65887,
#65888,#65889,#65890,#65891,#65892,#65893,#65894,#65895,#65896,#65897,#65898,
#65899,#65900,#65901,#65902,#65903,#65904,#65905,#65906,#65907,#65908,#65909,
#65910,#65911,#65912,#65913,#65914,#65915,#65916,#65917,#65918,#65919,#65920,
#65921,#65922,#65923,#65924,#65925,#65926,#65927,#65928,#65929,#65930,#65931,
#65932,#65933,#65934,#65935,#65936,#65937,#65938,#65939,#65940,#65941,#65942,
#65943),.UNSPECIFIED.,.F.,.F.,(4,3,3,3,3,3,3,3,3,3,3,3,3,3,3,3,3,3,3,3,
3,3,3,3,3,3,3,3,3,3,3,3,3,3,3,3,3,3,3,3,3,3,3,3,3,3,3,3,3,3,3,3,3,3,3,3,
3,3,3,3,3,3,3,3,3,3,3,3,3,3,3,3,3,3,3,4),(-230.287419852317,-230.186349361613,
-230.084766015855,-229.982553557715,-229.934370758751,-229.845818606672,
-229.757381211149,-229.669034767952,-229.577237434868,-229.488993312962,
-229.400762627027,-229.312524008303,-229.224256087456,-229.135887786815,
-229.047459975654,-228.958901839552,-228.934656103279,-228.846103951199,
-228.757666555676,-228.669320112478,-228.577522779394,-228.489278657488,
-228.401047971552,-228.312809352828,-228.224541431979,-228.136173131338,
-228.047745320177,-227.959187184074,-227.934941447806,-227.846389295726,
-227.757951900203,-227.669605457005,-227.577808123921,-227.489564002014,
-227.401333316078,-227.313094697354,-227.224826776505,-227.136458475864,
-227.048030664703,-226.9594725286,-226.935226792333,-226.846674640253,-226.75823724473,
-226.669890801532,-226.578093468448,-226.489849346542,-226.401618660606,
-226.313380041883,-226.225112121034,-226.136743820393,-226.048316009232,
-225.959757873129,-225.93551213686,-225.84695998478,-225.758522589257,-225.670176146059,
-225.578378812975,-225.490134691069,-225.401904005132,-225.313665386408,
-225.22539746556,-225.137029164918,-225.048601353757,-224.960043217654,
-224.935797481387,-224.848106940113,-224.760530424475,-224.673043217952,
-224.585619196174,-224.498227872774,-224.410847062648,-224.323454593684,
-224.235978024256,-224.148456092247,-224.060803396832,-224.00423479148),
 .UNSPECIFIED.);
#443=B_SPLINE_CURVE_WITH_KNOTS('',3,(#65945,#65946,#65947,#65948,#65949,
#65950,#65951,#65952,#65953,#65954,#65955,#65956),.UNSPECIFIED.,.F.,.F.,
(4,2,1,1,1,1,1,1,4),(-224.00423479148,-223.936082825914,-222.936368170442,
-221.936653514969,-220.936938859496,-219.937224204023,-218.93750954855,
-217.937794893077,-217.7210494843),.UNSPECIFIED.);
#444=B_SPLINE_CURVE_WITH_KNOTS('',3,(#65958,#65959,#65960,#65961,#65962,
#65963,#65964,#65965,#65966,#65967),.UNSPECIFIED.,.F.,.F.,(4,1,1,1,1,1,
1,4),(-217.7210494843,-216.938080237605,-215.938365582132,-214.938650926659,
-213.938936271186,-212.939221615713,-211.93950696024,-211.43786417712),
 .UNSPECIFIED.);
#445=B_SPLINE_CURVE_WITH_KNOTS('',3,(#65969,#65970,#65971,#65972,#65973,
#65974,#65975,#65976,#65977,#65978),.UNSPECIFIED.,.F.,.F.,(4,1,1,1,1,1,
1,4),(-211.43786417712,-210.939792304768,-209.940077649295,-208.940362993822,
-207.940648338349,-206.940933682876,-205.941219027403,-205.154678869941),
 .UNSPECIFIED.);
#446=B_SPLINE_CURVE_WITH_KNOTS('',3,(#65980,#65981,#65982,#65983,#65984,
#65985,#65986,#65987,#65988,#65989,#65990),.UNSPECIFIED.,.F.,.F.,(4,1,1,
1,1,1,1,1,4),(-205.154678869941,-204.941504371931,-203.941789716458,-202.942075060985,
-201.942360405512,-200.942645750039,-199.942931094566,-198.943216439094,
-198.871493562761),.UNSPECIFIED.);
#447=B_SPLINE_CURVE_WITH_KNOTS('',3,(#65992,#65993,#65994,#65995,#65996,
#65997,#65998,#65999,#66000,#66001,#66002,#66003,#66004,#66005,#66006,#66007,
#66008,#66009,#66010,#66011,#66012,#66013,#66014,#66015,#66016,#66017,#66018,
#66019,#66020,#66021,#66022,#66023,#66024,#66025,#66026,#66027,#66028,#66029,
#66030,#66031,#66032,#66033,#66034,#66035,#66036,#66037,#66038,#66039,#66040,
#66041,#66042,#66043,#66044,#66045,#66046,#66047,#66048,#66049,#66050,#66051,
#66052,#66053,#66054,#66055,#66056,#66057,#66058,#66059,#66060,#66061,#66062,
#66063,#66064,#66065,#66066,#66067,#66068,#66069,#66070,#66071,#66072,#66073,
#66074,#66075,#66076,#66077,#66078,#66079,#66080,#66081,#66082,#66083,#66084,
#66085,#66086,#66087,#66088,#66089,#66090,#66091,#66092,#66093,#66094,#66095,
#66096,#66097,#66098,#66099,#66100,#66101,#66102,#66103,#66104,#66105,#66106,
#66107,#66108,#66109,#66110,#66111,#66112,#66113,#66114,#66115,#66116,#66117,
#66118,#66119,#66120,#66121,#66122,#66123,#66124,#66125,#66126,#66127,#66128,
#66129,#66130,#66131,#66132,#66133,#66134,#66135,#66136,#66137,#66138,#66139,
#66140,#66141,#66142,#66143,#66144,#66145,#66146,#66147,#66148,#66149,#66150,
#66151,#66152,#66153,#66154,#66155,#66156,#66157,#66158,#66159,#66160,#66161,
#66162,#66163,#66164,#66165,#66166,#66167,#66168,#66169,#66170,#66171,#66172,
#66173,#66174,#66175,#66176,#66177,#66178,#66179,#66180,#66181,#66182,#66183,
#66184,#66185,#66186,#66187,#66188,#66189,#66190,#66191,#66192,#66193,#66194,
#66195,#66196,#66197,#66198,#66199,#66200,#66201,#66202,#66203,#66204,#66205,
#66206,#66207,#66208,#66209,#66210,#66211,#66212,#66213,#66214,#66215,#66216,
#66217),.UNSPECIFIED.,.F.,.F.,(4,3,3,3,3,3,3,3,3,3,3,3,3,3,3,3,3,3,3,3,
3,3,3,3,3,3,3,3,3,3,3,3,3,3,3,3,3,3,3,3,3,3,3,3,3,3,3,3,3,3,3,3,3,3,3,3,
3,3,3,3,3,3,3,3,3,3,3,3,3,3,3,3,3,3,3,4),(-198.871493562761,-198.783864600819,
-198.696343722576,-198.608906209389,-198.521523012626,-198.434166966534,
-198.346815865093,-198.259447510499,-198.171987253728,-198.084476748613,
-197.996829867738,-197.943501783621,-197.854949631541,-197.766512236018,
-197.67816579282,-197.586368459736,-197.49812433783,-197.409893651894,-197.32165503317,
-197.233387112322,-197.145018811681,-197.05659100052,-196.968032864417,
-196.943787128148,-196.855234976068,-196.766797580545,-196.678451137347,
-196.586653804263,-196.498409682357,-196.410178996421,-196.321940377697,
-196.233672456848,-196.145304156207,-196.056876345046,-195.968318208943,
-195.944072472675,-195.855520320595,-195.767082925072,-195.678736481874,
-195.58693914879,-195.498695026884,-195.410464340948,-195.322225722224,
-195.233957801376,-195.145589500735,-195.057161689573,-194.968603553471,
-194.944357817202,-194.855805665122,-194.767368269599,-194.679021826401,
-194.587224493317,-194.498980371411,-194.410749685474,-194.32251106675,
-194.234243145902,-194.14587484526,-194.057447034099,-193.968888897996,
-193.944643161729,-193.856091009649,-193.767653614126,-193.679307170928,
-193.587509837844,-193.499265715939,-193.411035030003,-193.322796411279,
-193.234528490431,-193.14616018979,-193.057732378629,-192.969174242526,
-192.944928506257,-192.843104874923,-192.741682446818,-192.640994115083,
-192.588308503375),.UNSPECIFIED.);
#448=B_SPLINE_CURVE_WITH_KNOTS('',3,(#66219,#66220,#66221,#66222,#66223,
#66224,#66225,#66226,#66227,#66228),.UNSPECIFIED.,.F.,.F.,(4,1,1,1,1,1,
1,4),(-192.588308255582,-191.945213850784,-190.945499195311,-189.945784539838,
-188.946069884365,-187.946355228892,-186.94664057342,-186.305122948402),
 .UNSPECIFIED.);
#449=B_SPLINE_CURVE_WITH_KNOTS('',3,(#66230,#66231,#66232,#66233,#66234,
#66235,#66236,#66237,#66238,#66239,#66240,#66241,#66242,#66243,#66244,#66245,
#66246,#66247,#66248,#66249,#66250,#66251,#66252,#66253,#66254,#66255,#66256,
#66257,#66258,#66259,#66260,#66261,#66262,#66263,#66264,#66265,#66266,#66267,
#66268,#66269,#66270,#66271,#66272,#66273,#66274,#66275,#66276,#66277,#66278,
#66279,#66280,#66281,#66282,#66283,#66284,#66285,#66286,#66287,#66288,#66289,
#66290,#66291,#66292,#66293,#66294,#66295,#66296,#66297,#66298,#66299,#66300,
#66301,#66302,#66303,#66304,#66305,#66306,#66307,#66308,#66309,#66310,#66311,
#66312,#66313,#66314,#66315,#66316,#66317,#66318,#66319,#66320,#66321,#66322,
#66323,#66324,#66325,#66326,#66327,#66328,#66329,#66330,#66331,#66332,#66333,
#66334,#66335,#66336,#66337,#66338,#66339,#66340,#66341,#66342,#66343,#66344,
#66345,#66346,#66347,#66348,#66349,#66350,#66351,#66352,#66353,#66354,#66355,
#66356,#66357,#66358,#66359,#66360,#66361,#66362,#66363,#66364,#66365,#66366,
#66367,#66368,#66369,#66370,#66371,#66372,#66373,#66374,#66375,#66376,#66377,
#66378,#66379,#66380,#66381,#66382,#66383,#66384,#66385,#66386,#66387,#66388,
#66389,#66390,#66391,#66392,#66393,#66394,#66395,#66396,#66397,#66398,#66399,
#66400,#66401,#66402,#66403,#66404,#66405,#66406,#66407,#66408,#66409,#66410,
#66411,#66412,#66413,#66414,#66415,#66416,#66417,#66418,#66419,#66420,#66421,
#66422,#66423,#66424,#66425,#66426,#66427,#66428,#66429,#66430,#66431,#66432,
#66433,#66434,#66435,#66436,#66437,#66438,#66439,#66440,#66441,#66442,#66443,
#66444,#66445,#66446,#66447,#66448,#66449,#66450,#66451,#66452,#66453,#66454,
#66455),.UNSPECIFIED.,.F.,.F.,(4,3,3,3,3,3,3,3,3,3,3,3,3,3,3,3,3,3,3,3,
3,3,3,3,3,3,3,3,3,3,3,3,3,3,3,3,3,3,3,3,3,3,3,3,3,3,3,3,3,3,3,3,3,3,3,3,
3,3,3,3,3,3,3,3,3,3,3,3,3,3,3,3,3,3,3,4),(-186.305122700355,-186.204477591045,
-186.103348556496,-186.0016110299,-185.946925917947,-185.858373765867,-185.769936370344,
-185.681589927145,-185.589792594061,-185.501548472155,-185.413317786219,
-185.325079167494,-185.236811246646,-185.148442946004,-185.060015134843,
-184.97145699874,-184.947211262474,-184.858659110394,-184.770221714871,
-184.681875271673,-184.590077938589,-184.501833816683,-184.413603130747,
-184.325364512023,-184.237096591174,-184.148728290533,-184.060300479372,
-183.971742343269,-183.947496607001,-183.858944454921,-183.770507059398,
-183.6821606162,-183.590363283116,-183.50211916121,-183.413888475274,-183.32564985655,
-183.237381935702,-183.149013635061,-183.0605858239,-182.972027687797,-182.947781951528,
-182.859229799448,-182.770792403925,-182.682445960727,-182.590648627643,
-182.502404505736,-182.4141738198,-182.325935201076,-182.237667280228,-182.149298979586,
-182.060871168425,-181.972313032322,-181.948067296055,-181.859515143976,
-181.771077748453,-181.682731305255,-181.590933972171,-181.502689850265,
-181.414459164329,-181.326220545605,-181.237952624757,-181.149584324116,
-181.061156512955,-180.972598376852,-180.948352640583,-180.860708602494,
-180.773178543556,-180.685737705076,-180.598360004986,-180.511014872504,
-180.42368008632,-180.336333438008,-180.248903392421,-180.161427705554,
-180.073823597944,-180.021937641223),.UNSPECIFIED.);
#450=B_SPLINE_CURVE_WITH_KNOTS('',3,(#66457,#66458,#66459,#66460,#66461,
#66462,#66463,#66464,#66465,#66466,#66467),.UNSPECIFIED.,.F.,.F.,(4,1,1,
1,1,1,1,1,4),(-180.021937641223,-179.94863798511,-178.948923329637,-177.949208674164,
-176.949494018691,-175.949779363218,-174.950064707746,-173.950350052273,
-173.738752334043),.UNSPECIFIED.);
#451=B_SPLINE_CURVE_WITH_KNOTS('',3,(#66469,#66470,#66471,#66472,#66473,
#66474,#66475,#66476,#66477,#66478,#66479,#66480,#66481,#66482,#66483,#66484,
#66485,#66486,#66487,#66488,#66489,#66490,#66491,#66492,#66493,#66494,#66495,
#66496,#66497,#66498,#66499,#66500,#66501,#66502,#66503,#66504,#66505,#66506,
#66507,#66508,#66509,#66510,#66511,#66512,#66513,#66514,#66515,#66516,#66517,
#66518,#66519,#66520,#66521,#66522,#66523,#66524,#66525,#66526,#66527,#66528,
#66529,#66530,#66531,#66532,#66533,#66534,#66535,#66536,#66537,#66538,#66539,
#66540,#66541,#66542,#66543,#66544,#66545,#66546,#66547,#66548,#66549,#66550,
#66551,#66552,#66553,#66554,#66555,#66556,#66557,#66558,#66559,#66560,#66561,
#66562,#66563,#66564,#66565,#66566,#66567,#66568,#66569,#66570,#66571,#66572,
#66573,#66574,#66575,#66576,#66577,#66578,#66579,#66580,#66581,#66582,#66583,
#66584,#66585,#66586,#66587,#66588,#66589,#66590,#66591,#66592,#66593,#66594,
#66595,#66596,#66597,#66598,#66599,#66600,#66601,#66602,#66603,#66604,#66605,
#66606,#66607,#66608,#66609,#66610,#66611,#66612,#66613,#66614,#66615,#66616,
#66617,#66618,#66619,#66620,#66621,#66622,#66623,#66624,#66625,#66626,#66627,
#66628,#66629,#66630,#66631,#66632,#66633,#66634,#66635,#66636,#66637,#66638,
#66639,#66640,#66641,#66642,#66643,#66644,#66645,#66646,#66647,#66648,#66649,
#66650,#66651,#66652,#66653,#66654,#66655,#66656,#66657,#66658,#66659,#66660,
#66661,#66662,#66663,#66664,#66665,#66666,#66667,#66668,#66669,#66670,#66671,
#66672,#66673,#66674,#66675,#66676,#66677,#66678,#66679,#66680,#66681,#66682,
#66683,#66684,#66685,#66686,#66687,#66688,#66689,#66690,#66691,#66692,#66693,
#66694),.UNSPECIFIED.,.F.,.F.,(4,3,3,3,3,3,3,3,3,3,3,3,3,3,3,3,3,3,3,3,
3,3,3,3,3,3,3,3,3,3,3,3,3,3,3,3,3,3,3,3,3,3,3,3,3,3,3,3,3,3,3,3,3,3,3,3,
3,3,3,3,3,3,3,3,3,3,3,3,3,3,3,3,3,3,3,4),(-173.738752334043,-173.651614929709,
-173.563992488095,-173.476967882539,-173.389960097741,-173.302946680709,
-173.214868859732,-173.127730364889,-173.039182880844,-172.9506353968,-172.86208324472,
-172.773645849197,-172.685299405999,-172.593502072915,-172.505257951009,
-172.417027265073,-172.328788646349,-172.240520725501,-172.152152424859,
-172.063724613698,-171.975166477595,-171.950920741327,-171.862368589247,
-171.773931193724,-171.685584750526,-171.593787417442,-171.505543295536,
-171.4173126096,-171.329073990876,-171.240806070027,-171.152437769386,-171.064009958225,
-170.975451822122,-170.951206085854,-170.862653933774,-170.774216538251,
-170.685870095053,-170.594072761969,-170.505828640062,-170.417597954126,
-170.329359335402,-170.241091414554,-170.152723113912,-170.064295302751,
-169.975737166648,-169.951491430381,-169.862939278302,-169.774501882779,
-169.686155439581,-169.594358106497,-169.506113984591,-169.417883298655,
-169.329644679931,-169.241376759083,-169.153008458442,-169.064580647281,
-168.976022511178,-168.951776774909,-168.86322462283,-168.774787227306,
-168.686440784108,-168.594643451024,-168.506399329118,-168.418168643182,
-168.329930024459,-168.241662103611,-168.15329380297,-168.064865991809,
-167.976307855706,-167.952062119436,-167.858803568459,-167.765717118764,
-167.672853547193,-167.580125408874,-167.487567112195,-167.455567027009),
 .UNSPECIFIED.);
#452=B_SPLINE_CURVE_WITH_KNOTS('',3,(#66696,#66697,#66698,#66699,#66700,
#66701,#66702,#66703,#66704,#66705,#66706,#66707,#66708,#66709,#66710,#66711,
#66712,#66713,#66714,#66715,#66716,#66717,#66718,#66719,#66720,#66721,#66722,
#66723,#66724,#66725,#66726,#66727,#66728,#66729,#66730,#66731,#66732,#66733,
#66734,#66735,#66736,#66737,#66738,#66739,#66740,#66741,#66742,#66743,#66744,
#66745,#66746,#66747,#66748,#66749,#66750,#66751,#66752,#66753,#66754,#66755,
#66756,#66757,#66758,#66759,#66760,#66761,#66762,#66763,#66764,#66765,#66766,
#66767,#66768,#66769,#66770,#66771,#66772,#66773,#66774,#66775,#66776,#66777,
#66778,#66779,#66780,#66781,#66782,#66783,#66784,#66785,#66786,#66787,#66788,
#66789,#66790,#66791,#66792,#66793,#66794,#66795,#66796,#66797,#66798,#66799,
#66800,#66801,#66802,#66803,#66804,#66805,#66806,#66807,#66808,#66809,#66810,
#66811,#66812,#66813,#66814,#66815,#66816,#66817,#66818,#66819,#66820,#66821,
#66822,#66823,#66824,#66825,#66826,#66827,#66828,#66829,#66830,#66831,#66832,
#66833,#66834,#66835,#66836,#66837,#66838,#66839,#66840,#66841,#66842,#66843,
#66844,#66845,#66846,#66847,#66848,#66849,#66850,#66851,#66852,#66853,#66854,
#66855,#66856,#66857,#66858,#66859,#66860,#66861,#66862,#66863,#66864,#66865,
#66866,#66867,#66868,#66869,#66870,#66871,#66872,#66873,#66874,#66875,#66876,
#66877,#66878,#66879,#66880,#66881,#66882,#66883,#66884,#66885,#66886,#66887,
#66888,#66889,#66890,#66891,#66892,#66893,#66894,#66895,#66896,#66897,#66898,
#66899,#66900,#66901,#66902,#66903,#66904,#66905,#66906,#66907,#66908,#66909,
#66910,#66911,#66912,#66913,#66914,#66915,#66916,#66917,#66918,#66919,#66920,
#66921),.UNSPECIFIED.,.F.,.F.,(4,3,3,3,3,3,3,3,3,3,3,3,3,3,3,3,3,3,3,3,
3,3,3,3,3,3,3,3,3,3,3,3,3,3,3,3,3,3,3,3,3,3,3,3,3,3,3,3,3,3,3,3,3,3,3,3,
3,3,3,3,3,3,3,3,3,3,3,3,3,3,3,3,3,3,3,4),(-167.455567026863,-167.363266863581,
-167.270842710716,-167.178199114077,-167.085435326711,-166.992463354601,
-166.952347463963,-166.863795311883,-166.77535791636,-166.687011473162,
-166.595214140078,-166.506970018171,-166.418739332235,-166.330500713511,
-166.242232792663,-166.153864492021,-166.06543668086,-165.976878544757,
-165.95263280849,-165.86408065641,-165.775643260887,-165.687296817689,-165.595499484605,
-165.507255362699,-165.419024676763,-165.330786058039,-165.24251813719,
-165.154149836549,-165.065722025388,-164.977163889285,-164.952918153017,
-164.864366000937,-164.775928605414,-164.687582162216,-164.595784829132,
-164.507540707226,-164.41931002129,-164.331071402566,-164.242803481717,
-164.154435181076,-164.066007369915,-163.977449233812,-163.953203497544,
-163.864651345465,-163.776213949942,-163.687867506743,-163.59607017366,
-163.507826051754,-163.419595365818,-163.331356747094,-163.243088826246,
-163.154720525604,-163.066292714444,-162.977734578341,-162.953488842072,
-162.864936689992,-162.776499294469,-162.688152851271,-162.596355518187,
-162.508111396281,-162.419880710345,-162.331642091621,-162.243374170773,
-162.155005870132,-162.066578058971,-161.978019922868,-161.953774186599,
-161.866428726277,-161.779222289971,-161.692095142986,-161.605024747212,
-161.517988622192,-161.430932553615,-161.343870414659,-161.256723427662,
-161.172381719684),.UNSPECIFIED.);
#453=B_SPLINE_CURVE_WITH_KNOTS('',3,(#66923,#66924,#66925,#66926,#66927,
#66928,#66929,#66930,#66931,#66932,#66933),.UNSPECIFIED.,.F.,.F.,(4,1,1,
1,1,1,1,1,4),(-161.172381719684,-160.954059531126,-159.954344875653,-158.95463022018,
-157.954915564707,-156.955200909235,-155.955486253762,-154.955771598289,
-154.889196412504),.UNSPECIFIED.);
#454=B_SPLINE_CURVE_WITH_KNOTS('',3,(#66935,#66936,#66937,#66938,#66939,
#66940,#66941,#66942,#66943,#66944,#66945,#66946,#66947,#66948,#66949,#66950,
#66951,#66952,#66953,#66954,#66955,#66956,#66957,#66958,#66959,#66960,#66961,
#66962,#66963,#66964,#66965,#66966,#66967,#66968,#66969,#66970,#66971,#66972,
#66973,#66974,#66975,#66976,#66977,#66978,#66979,#66980,#66981,#66982,#66983,
#66984,#66985,#66986,#66987,#66988,#66989,#66990,#66991,#66992,#66993,#66994,
#66995,#66996,#66997,#66998,#66999,#67000,#67001,#67002,#67003,#67004,#67005,
#67006,#67007,#67008,#67009,#67010,#67011,#67012,#67013,#67014,#67015,#67016,
#67017,#67018,#67019,#67020,#67021,#67022,#67023,#67024,#67025,#67026,#67027,
#67028,#67029,#67030,#67031,#67032,#67033,#67034,#67035,#67036,#67037,#67038,
#67039,#67040,#67041,#67042,#67043,#67044,#67045,#67046,#67047,#67048,#67049,
#67050,#67051,#67052,#67053,#67054,#67055,#67056,#67057,#67058,#67059,#67060,
#67061,#67062,#67063,#67064,#67065,#67066,#67067,#67068,#67069,#67070,#67071,
#67072,#67073,#67074,#67075,#67076,#67077,#67078,#67079,#67080,#67081,#67082,
#67083,#67084,#67085,#67086,#67087,#67088,#67089,#67090,#67091,#67092,#67093,
#67094,#67095,#67096,#67097,#67098,#67099,#67100,#67101,#67102,#67103,#67104,
#67105,#67106,#67107,#67108,#67109,#67110,#67111,#67112,#67113,#67114,#67115,
#67116,#67117,#67118,#67119,#67120,#67121,#67122,#67123,#67124,#67125,#67126,
#67127,#67128,#67129,#67130,#67131,#67132,#67133,#67134,#67135,#67136,#67137,
#67138,#67139,#67140,#67141,#67142,#67143,#67144,#67145,#67146,#67147,#67148,
#67149,#67150,#67151,#67152,#67153,#67154,#67155,#67156,#67157,#67158,#67159,
#67160),.UNSPECIFIED.,.F.,.F.,(4,3,3,3,3,3,3,3,3,3,3,3,3,3,3,3,3,3,3,3,
3,3,3,3,3,3,3,3,3,3,3,3,3,3,3,3,3,3,3,3,3,3,3,3,3,3,3,3,3,3,3,3,3,3,3,3,
3,3,3,3,3,3,3,3,3,3,3,3,3,3,3,3,3,3,3,4),(-154.889196412504,-154.801516541426,
-154.713945565697,-154.62645880606,-154.539027538957,-154.451624262389,
-154.364226806844,-154.276813011792,-154.189307658123,-154.101752947617,
-154.014060389313,-153.956056942816,-153.867504790736,-153.779067395213,
-153.690720952015,-153.598923618931,-153.510679497025,-153.422448811088,
-153.334210192364,-153.245942271516,-153.157573970875,-153.069146159713,
-152.98058802361,-152.956342287343,-152.867790135264,-152.779352739741,
-152.691006296543,-152.599208963459,-152.510964841553,-152.422734155617,
-152.334495536893,-152.246227616045,-152.157859315404,-152.069431504243,
-151.98087336814,-151.956627631871,-151.868075479791,-151.779638084268,
-151.69129164107,-151.599494307986,-151.51125018608,-151.423019500144,-151.33478088142,
-151.246512960572,-151.158144659931,-151.06971684877,-150.981158712667,
-150.956912976398,-150.868360824318,-150.779923428795,-150.691576985597,
-150.599779652513,-150.511535530607,-150.42330484467,-150.335066225946,
-150.246798305098,-150.158430004457,-150.070002193295,-149.981444057192,
-149.957198320925,-149.868646168845,-149.780208773322,-149.691862330124,
-149.60006499704,-149.511820875134,-149.423590189197,-149.335351570474,
-149.247083649626,-149.158715348984,-149.070287537824,-148.981729401721,
-148.957483665452,-148.855191749666,-148.753322456798,-148.652222206138,
-148.606011351141),.UNSPECIFIED.);
#455=B_SPLINE_CURVE_WITH_KNOTS('',3,(#67162,#67163,#67164,#67165,#67166,
#67167,#67168,#67169,#67170,#67171),.UNSPECIFIED.,.F.,.F.,(4,1,1,1,1,1,
1,4),(-148.606011105325,-147.957769009979,-146.958054354506,-145.958339699033,
-144.958625043561,-143.958910388088,-142.959195732615,-142.322825798145),
 .UNSPECIFIED.);
#456=B_SPLINE_CURVE_WITH_KNOTS('',3,(#67173,#67174,#67175,#67176,#67177,
#67178,#67179,#67180,#67181,#67182),.UNSPECIFIED.,.F.,.F.,(4,1,1,1,1,1,
1,4),(-142.322825798145,-141.959481077142,-140.959766421669,-139.960051766196,
-138.960337110724,-137.960622455251,-136.960907799778,-136.039640490966),
 .UNSPECIFIED.);
#457=B_SPLINE_CURVE_WITH_KNOTS('',3,(#67184,#67185,#67186,#67187,#67188,
#67189,#67190,#67191,#67192,#67193,#67194,#67195),.UNSPECIFIED.,.F.,.F.,
(4,2,1,1,1,1,1,1,4),(-136.039640490966,-135.961193144305,-134.961478488832,
-133.961763833359,-132.962049177887,-131.962334522414,-130.962619866941,
-129.962905211468,-129.756455183786),.UNSPECIFIED.);
#458=B_SPLINE_CURVE_WITH_KNOTS('',3,(#67197,#67198,#67199,#67200,#67201,
#67202,#67203,#67204,#67205,#67206,#67207,#67208,#67209,#67210,#67211,#67212,
#67213,#67214,#67215,#67216,#67217,#67218,#67219,#67220,#67221,#67222,#67223,
#67224,#67225,#67226,#67227,#67228,#67229,#67230,#67231,#67232,#67233,#67234,
#67235,#67236,#67237,#67238,#67239,#67240,#67241,#67242,#67243,#67244,#67245,
#67246,#67247,#67248,#67249,#67250,#67251,#67252,#67253,#67254,#67255,#67256,
#67257,#67258,#67259,#67260,#67261,#67262,#67263,#67264,#67265,#67266,#67267,
#67268,#67269,#67270,#67271,#67272,#67273,#67274,#67275,#67276,#67277,#67278,
#67279,#67280,#67281,#67282,#67283,#67284,#67285,#67286,#67287,#67288,#67289,
#67290,#67291,#67292,#67293,#67294,#67295,#67296,#67297,#67298,#67299,#67300,
#67301,#67302,#67303,#67304,#67305,#67306,#67307,#67308,#67309,#67310,#67311,
#67312,#67313,#67314,#67315,#67316,#67317,#67318,#67319,#67320,#67321,#67322,
#67323,#67324,#67325,#67326,#67327,#67328,#67329,#67330,#67331,#67332,#67333,
#67334,#67335,#67336,#67337,#67338,#67339,#67340,#67341,#67342,#67343,#67344,
#67345,#67346,#67347,#67348,#67349,#67350,#67351,#67352,#67353,#67354,#67355,
#67356,#67357,#67358,#67359,#67360,#67361,#67362,#67363,#67364,#67365,#67366,
#67367,#67368,#67369,#67370,#67371,#67372,#67373,#67374,#67375,#67376,#67377,
#67378,#67379,#67380,#67381,#67382,#67383,#67384,#67385,#67386,#67387,#67388,
#67389,#67390,#67391,#67392,#67393,#67394,#67395,#67396,#67397,#67398,#67399,
#67400,#67401,#67402,#67403,#67404,#67405,#67406,#67407,#67408,#67409,#67410,
#67411,#67412,#67413,#67414,#67415,#67416,#67417,#67418,#67419,#67420,#67421,
#67422),.UNSPECIFIED.,.F.,.F.,(4,3,3,3,3,3,3,3,3,3,3,3,3,3,3,3,3,3,3,3,
3,3,3,3,3,3,3,3,3,3,3,3,3,3,3,3,3,3,3,3,3,3,3,3,3,3,3,3,3,3,3,3,3,3,3,3,
3,3,3,3,3,3,3,3,3,3,3,3,3,3,3,3,3,3,3,4),(-129.756455183786,-129.669330401864,
-129.58106292113,-129.494055101733,-129.407065460323,-129.320071530291,
-129.230851286717,-129.143733708822,-129.053462132409,-128.963190555995,
-128.874638403916,-128.786201008393,-128.697854565195,-128.606057232111,
-128.517813110205,-128.429582424269,-128.341343805545,-128.253075884698,
-128.164707584056,-128.076279772896,-127.987721636793,-127.963475900523,
-127.874923748443,-127.78648635292,-127.698139909722,-127.606342576638,
-127.518098454732,-127.429867768796,-127.341629150072,-127.253361229224,
-127.164992928583,-127.076565117422,-126.988006981319,-126.96376124505,
-126.87520909297,-126.786771697447,-126.698425254249,-126.606627921165,
-126.518383799259,-126.430153113322,-126.341914494598,-126.25364657375,
-126.165278273108,-126.076850461947,-125.988292325844,-125.964046589577,
-125.875494437497,-125.787057041974,-125.698710598776,-125.606913265692,
-125.518669143786,-125.43043845785,-125.342199839126,-125.253931918278,
-125.165563617636,-125.077135806475,-124.988577670373,-124.964331934104,
-124.875779782024,-124.787342386501,-124.698995943303,-124.607198610219,
-124.518954488313,-124.430723802377,-124.342485183653,-124.254217262805,
-124.165848962164,-124.077421151002,-123.9888630149,-123.964617278631,-123.871137501164,
-123.777833647348,-123.684759513492,-123.591825941801,-123.49906942334,
-123.473269876792),.UNSPECIFIED.);
#459=B_SPLINE_CURVE_WITH_KNOTS('',3,(#67424,#67425,#67426,#67427,#67428,
#67429,#67430,#67431,#67432,#67433,#67434,#67435,#67436,#67437,#67438,#67439,
#67440,#67441,#67442,#67443,#67444,#67445,#67446,#67447,#67448,#67449,#67450,
#67451,#67452,#67453,#67454,#67455,#67456,#67457,#67458,#67459,#67460,#67461,
#67462,#67463,#67464,#67465,#67466,#67467,#67468,#67469,#67470,#67471,#67472,
#67473,#67474,#67475,#67476,#67477,#67478,#67479,#67480,#67481,#67482,#67483,
#67484,#67485,#67486,#67487,#67488,#67489,#67490,#67491,#67492,#67493,#67494,
#67495,#67496,#67497,#67498,#67499,#67500,#67501,#67502,#67503,#67504,#67505,
#67506,#67507,#67508,#67509,#67510,#67511,#67512,#67513,#67514,#67515,#67516,
#67517,#67518,#67519,#67520,#67521,#67522,#67523,#67524,#67525,#67526,#67527,
#67528,#67529,#67530,#67531,#67532,#67533,#67534,#67535,#67536,#67537,#67538,
#67539,#67540,#67541,#67542,#67543,#67544,#67545,#67546,#67547,#67548,#67549,
#67550,#67551,#67552,#67553,#67554,#67555,#67556,#67557,#67558,#67559,#67560,
#67561,#67562,#67563,#67564,#67565,#67566,#67567,#67568,#67569,#67570,#67571,
#67572,#67573,#67574,#67575,#67576,#67577,#67578,#67579,#67580,#67581,#67582,
#67583,#67584,#67585,#67586,#67587,#67588,#67589,#67590,#67591,#67592,#67593,
#67594,#67595,#67596,#67597,#67598,#67599,#67600,#67601,#67602,#67603,#67604,
#67605,#67606,#67607,#67608,#67609,#67610,#67611,#67612,#67613,#67614,#67615,
#67616,#67617,#67618,#67619,#67620,#67621,#67622,#67623,#67624,#67625,#67626,
#67627,#67628,#67629,#67630,#67631,#67632,#67633,#67634,#67635,#67636,#67637,
#67638,#67639,#67640,#67641,#67642,#67643,#67644,#67645,#67646,#67647,#67648,
#67649),.UNSPECIFIED.,.F.,.F.,(4,3,3,3,3,3,3,3,3,3,3,3,3,3,3,3,3,3,3,3,
3,3,3,3,3,3,3,3,3,3,3,3,3,3,3,3,3,3,3,3,3,3,3,3,3,3,3,3,3,3,3,3,3,3,3,3,
3,3,3,3,3,3,3,3,3,3,3,3,3,3,3,3,3,3,3,4),(-123.473269876606,-123.381161277955,
-123.288935985714,-123.196498304588,-123.103945159693,-123.011185121163,
-122.964902623158,-122.876350471079,-122.787913075556,-122.699566632358,
-122.607769299274,-122.519525177368,-122.431294491433,-122.343055872709,
-122.254787951861,-122.16641965122,-122.077991840059,-121.989433703957,
-121.965187967686,-121.876635815606,-121.788198420083,-121.699851976885,
-121.608054643801,-121.519810521895,-121.431579835959,-121.343341217235,
-121.255073296387,-121.166704995745,-121.078277184585,-120.989719048482,
-120.965473312213,-120.876921160133,-120.78848376461,-120.700137321412,
-120.608339988328,-120.520095866422,-120.431865180485,-120.343626561761,
-120.255358640913,-120.166990340271,-120.07856252911,-119.990004393007,
-119.96575865674,-119.87720650466,-119.788769109137,-119.700422665939,-119.608625332855,
-119.520381210949,-119.432150525013,-119.343911906289,-119.255643985441,
-119.167275684799,-119.078847873638,-118.990289737535,-118.966044001267,
-118.877491849187,-118.789054453664,-118.700708010466,-118.608910677382,
-118.520666555476,-118.43243586954,-118.344197250816,-118.255929329967,
-118.167561029326,-118.079133218164,-117.990575082061,-117.966329345794,
-117.878958677332,-117.791727434839,-117.704575738324,-117.61748106669,
-117.530420956491,-117.44334239818,-117.356257991148,-117.269092049149,
-117.190084569427),.UNSPECIFIED.);
#460=B_SPLINE_CURVE_WITH_KNOTS('',3,(#67651,#67652,#67653,#67654,#67655,
#67656,#67657,#67658,#67659,#67660,#67661),.UNSPECIFIED.,.F.,.F.,(4,1,1,
1,1,1,1,1,4),(-117.190084569427,-116.966614690321,-115.966900034849,-114.967185379376,
-113.967470723903,-112.96775606843,-111.968041412957,-110.968326757484,
-110.906899262247),.UNSPECIFIED.);
#461=B_SPLINE_CURVE_WITH_KNOTS('',3,(#67663,#67664,#67665,#67666,#67667,
#67668,#67669,#67670,#67671,#67672,#67673,#67674,#67675,#67676,#67677,#67678,
#67679,#67680,#67681,#67682,#67683,#67684,#67685,#67686,#67687,#67688,#67689,
#67690,#67691,#67692,#67693,#67694,#67695,#67696,#67697,#67698,#67699,#67700,
#67701,#67702,#67703,#67704,#67705,#67706,#67707,#67708,#67709,#67710,#67711,
#67712,#67713,#67714,#67715,#67716,#67717,#67718,#67719,#67720,#67721,#67722,
#67723,#67724,#67725,#67726,#67727,#67728,#67729,#67730,#67731,#67732,#67733,
#67734,#67735,#67736,#67737,#67738,#67739,#67740,#67741,#67742,#67743,#67744,
#67745,#67746,#67747,#67748,#67749,#67750,#67751,#67752,#67753,#67754,#67755,
#67756,#67757,#67758,#67759,#67760,#67761,#67762,#67763,#67764,#67765,#67766,
#67767,#67768,#67769,#67770,#67771,#67772,#67773,#67774,#67775,#67776,#67777,
#67778,#67779,#67780,#67781,#67782,#67783,#67784,#67785,#67786,#67787,#67788,
#67789,#67790,#67791,#67792,#67793,#67794,#67795,#67796,#67797,#67798,#67799,
#67800,#67801,#67802,#67803,#67804,#67805,#67806,#67807,#67808,#67809,#67810,
#67811,#67812,#67813,#67814,#67815,#67816,#67817,#67818,#67819,#67820,#67821,
#67822,#67823,#67824,#67825,#67826,#67827,#67828,#67829,#67830,#67831,#67832,
#67833,#67834,#67835,#67836,#67837,#67838,#67839,#67840,#67841,#67842,#67843,
#67844,#67845,#67846,#67847,#67848,#67849,#67850,#67851,#67852,#67853,#67854,
#67855,#67856,#67857,#67858,#67859,#67860,#67861,#67862,#67863,#67864,#67865,
#67866,#67867,#67868,#67869,#67870,#67871,#67872,#67873,#67874,#67875,#67876,
#67877,#67878,#67879,#67880,#67881,#67882,#67883,#67884,#67885,#67886,#67887,
#67888),.UNSPECIFIED.,.F.,.F.,(4,3,3,3,3,3,3,3,3,3,3,3,3,3,3,3,3,3,3,3,
3,3,3,3,3,3,3,3,3,3,3,3,3,3,3,3,3,3,3,3,3,3,3,3,3,3,3,3,3,3,3,3,3,3,3,3,
3,3,3,3,3,3,3,3,3,3,3,3,3,3,3,3,3,3,3,4),(-110.906899262247,-110.81916613363,
-110.73154266842,-110.644004230026,-110.556522414419,-110.469069398607,
-110.381623052323,-110.294161255007,-110.20660822571,-110.119006713472,
-110.031265869715,-109.968612102012,-109.880059949932,-109.791622554409,
-109.703276111211,-109.611478778127,-109.523234656221,-109.435003970284,
-109.34676535156,-109.258497430712,-109.170129130071,-109.081701318909,
-108.993143182807,-108.968897446539,-108.880345294459,-108.791907898936,
-108.703561455738,-108.611764122654,-108.523520000748,-108.435289314812,
-108.347050696088,-108.258782775239,-108.170414474598,-108.081986663437,
-107.993428527334,-107.969182791066,-107.880630638987,-107.792193243463,
-107.703846800265,-107.612049467181,-107.523805345275,-107.435574659339,
-107.347336040615,-107.259068119767,-107.170699819126,-107.082272007965,
-106.993713871862,-106.969468135593,-106.880915983513,-106.79247858799,
-106.704132144792,-106.612334811708,-106.524090689802,-106.435860003866,
-106.347621385142,-106.259353464294,-106.170985163653,-106.082557352492,
-105.993999216389,-105.96975348012,-105.88120132804,-105.792763932517,-105.704417489319,
-105.612620156235,-105.524376034329,-105.436145348392,-105.347906729668,
-105.25963880882,-105.171270508178,-105.082842697018,-104.994284560914,
-104.970038824647,-104.867263249388,-104.764933531125,-104.663410117904,
-104.623714198583),.UNSPECIFIED.);
#462=B_SPLINE_CURVE_WITH_KNOTS('',3,(#67890,#67891,#67892,#67893,#67894,
#67895,#67896,#67897,#67898,#67899),.UNSPECIFIED.,.F.,.F.,(4,1,1,1,1,1,
1,4),(-104.623713955068,-103.970324169175,-102.970609513702,-101.970894858229,
-100.971180202756,-99.9714655472832,-98.9717508918104,-98.3405286478881),
 .UNSPECIFIED.);
#463=B_SPLINE_CURVE_WITH_KNOTS('',3,(#67901,#67902,#67903,#67904,#67905,
#67906,#67907,#67908,#67909,#67910),.UNSPECIFIED.,.F.,.F.,(4,1,1,1,1,1,
1,4),(-98.3405286478881,-97.9720362363375,-96.9723215808647,-95.9726069253919,
-94.972892269919,-93.9731776144462,-92.9734629589734,-92.0573433407085),
 .UNSPECIFIED.);
#464=B_SPLINE_CURVE_WITH_KNOTS('',3,(#67912,#67913,#67914,#67915,#67916,
#67917,#67918,#67919,#67920,#67921,#67922),.UNSPECIFIED.,.F.,.F.,(4,1,1,
1,1,1,1,1,4),(-92.0573433407085,-91.9737483035005,-90.9740336480277,-89.9743189925549,
-88.974604337082,-87.9748896816092,-86.9751750261364,-85.9754603706636,
-85.7741580335289),.UNSPECIFIED.);
#465=B_SPLINE_CURVE_WITH_KNOTS('',3,(#67924,#67925,#67926,#67927,#67928,
#67929,#67930,#67931,#67932,#67933,#67934,#67935,#67936,#67937,#67938,#67939,
#67940,#67941,#67942,#67943,#67944,#67945,#67946,#67947,#67948,#67949,#67950,
#67951,#67952,#67953,#67954,#67955,#67956,#67957,#67958,#67959,#67960,#67961,
#67962,#67963,#67964,#67965,#67966,#67967,#67968,#67969,#67970,#67971,#67972,
#67973,#67974,#67975,#67976,#67977,#67978,#67979,#67980,#67981,#67982,#67983,
#67984,#67985,#67986,#67987,#67988,#67989,#67990,#67991,#67992,#67993,#67994,
#67995,#67996,#67997,#67998,#67999,#68000,#68001,#68002,#68003,#68004,#68005,
#68006,#68007,#68008,#68009,#68010,#68011,#68012,#68013,#68014,#68015,#68016,
#68017,#68018,#68019,#68020,#68021,#68022,#68023,#68024,#68025,#68026,#68027,
#68028,#68029,#68030,#68031,#68032,#68033,#68034,#68035,#68036,#68037,#68038,
#68039,#68040,#68041,#68042,#68043,#68044,#68045,#68046,#68047,#68048,#68049,
#68050,#68051,#68052,#68053,#68054,#68055,#68056,#68057,#68058,#68059,#68060,
#68061,#68062,#68063,#68064,#68065,#68066,#68067,#68068,#68069,#68070,#68071,
#68072,#68073,#68074,#68075,#68076,#68077,#68078,#68079,#68080,#68081,#68082,
#68083,#68084,#68085,#68086,#68087,#68088,#68089,#68090,#68091,#68092,#68093,
#68094,#68095,#68096,#68097,#68098,#68099,#68100,#68101,#68102,#68103,#68104,
#68105,#68106,#68107,#68108,#68109,#68110,#68111,#68112,#68113,#68114,#68115,
#68116,#68117,#68118,#68119,#68120,#68121,#68122,#68123,#68124,#68125,#68126,
#68127,#68128,#68129,#68130,#68131,#68132,#68133,#68134,#68135,#68136,#68137,
#68138,#68139,#68140,#68141,#68142,#68143,#68144,#68145,#68146,#68147,#68148,
#68149,#68150,#68151,#68152),.UNSPECIFIED.,.F.,.F.,(4,3,3,3,3,3,3,3,3,3,
3,3,3,3,3,3,3,3,3,3,3,3,3,3,3,3,3,3,3,3,3,3,3,3,3,3,3,3,3,3,3,3,3,3,3,3,
3,3,3,3,3,3,3,3,3,3,3,3,3,3,3,3,3,3,3,3,3,3,3,3,3,3,3,3,3,3,4),(-85.7741580335289,
-85.687043478963,-85.5981312584914,-85.511137786955,-85.4241638250235,-85.3371868942073,
-85.2468265994532,-85.1597274426246,-85.0725693580145,-84.9852878854184,
-84.9757457151907,-84.8871935631111,-84.798756167588,-84.71040972439,-84.618612391306,
-84.5303682693999,-84.4421375834636,-84.3538989647399,-84.2656310438917,
-84.1772627432505,-84.0888349320897,-84.000276795987,-83.9760310597179,
-83.8874789076383,-83.7990415121153,-83.7106950689173,-83.6188977358333,
-83.5306536139271,-83.4424229279909,-83.3541843092672,-83.2659163884184,
-83.1775480877771,-83.089120276616,-83.0005621405133,-82.9763164042451,
-82.8877642521655,-82.7993268566425,-82.7109804134444,-82.6191830803604,
-82.5309389584542,-82.442708272518,-82.3544696537941,-82.2662017329457,
-82.1778334323044,-82.0894056211431,-82.0008474850403,-81.9766017487722,
-81.8880495966926,-81.7996122011695,-81.7112657579712,-81.6194684248872,
-81.5312243029812,-81.442993617045,-81.3547549983213,-81.2664870774732,
-81.178118776832,-81.0896909656709,-81.0011328295681,-80.9768870932994,
-80.8883349412198,-80.7998975456966,-80.7115511024986,-80.6197537694146,
-80.5315096475084,-80.4432789615722,-80.3550403428486,-80.2667724219998,
-80.1784041213586,-80.0899763101974,-80.0014181740946,-79.9771724378266,
-79.88346559413,-79.785342377222,-79.6920597431561,-79.5989227576672,-79.5059681543834,
-79.4909727264982),.UNSPECIFIED.);
#466=B_SPLINE_CURVE_WITH_KNOTS('',3,(#68154,#68155,#68156,#68157,#68158,
#68159,#68160,#68161,#68162,#68163,#68164,#68165,#68166,#68167,#68168,#68169,
#68170,#68171,#68172,#68173,#68174,#68175,#68176,#68177,#68178,#68179,#68180,
#68181,#68182,#68183,#68184,#68185,#68186,#68187,#68188,#68189,#68190,#68191,
#68192,#68193,#68194,#68195,#68196,#68197,#68198,#68199,#68200,#68201,#68202,
#68203,#68204,#68205,#68206,#68207,#68208,#68209,#68210,#68211,#68212,#68213,
#68214,#68215,#68216,#68217,#68218,#68219,#68220,#68221,#68222,#68223,#68224,
#68225,#68226,#68227,#68228,#68229,#68230,#68231,#68232,#68233,#68234,#68235,
#68236,#68237,#68238,#68239,#68240,#68241,#68242,#68243,#68244,#68245,#68246,
#68247,#68248,#68249,#68250,#68251,#68252,#68253,#68254,#68255,#68256,#68257,
#68258,#68259,#68260,#68261,#68262,#68263,#68264,#68265,#68266,#68267,#68268,
#68269,#68270,#68271,#68272,#68273,#68274,#68275,#68276,#68277,#68278,#68279,
#68280,#68281,#68282,#68283,#68284,#68285,#68286,#68287,#68288,#68289,#68290,
#68291,#68292,#68293,#68294,#68295,#68296,#68297,#68298,#68299,#68300,#68301,
#68302,#68303,#68304,#68305,#68306,#68307,#68308,#68309,#68310,#68311,#68312,
#68313,#68314,#68315,#68316,#68317,#68318,#68319,#68320,#68321,#68322,#68323,
#68324,#68325,#68326,#68327,#68328,#68329,#68330,#68331,#68332,#68333,#68334,
#68335,#68336,#68337,#68338,#68339,#68340,#68341,#68342,#68343,#68344,#68345,
#68346,#68347,#68348,#68349,#68350,#68351,#68352,#68353,#68354,#68355,#68356,
#68357,#68358,#68359,#68360,#68361,#68362,#68363,#68364,#68365,#68366,#68367,
#68368,#68369,#68370,#68371,#68372,#68373,#68374,#68375,#68376,#68377,#68378,
#68379),.UNSPECIFIED.,.F.,.F.,(4,3,3,3,3,3,3,3,3,3,3,3,3,3,3,3,3,3,3,3,
3,3,3,3,3,3,3,3,3,3,3,3,3,3,3,3,3,3,3,3,3,3,3,3,3,3,3,3,3,3,3,3,3,3,3,3,
3,3,3,3,3,3,3,3,3,3,3,3,3,3,3,3,3,3,3,4),(-79.4909727263493,-79.3990508671971,
-79.3070193033341,-79.2147821410095,-79.1224340910687,-79.0298803650998,
-78.9774577823537,-78.8889056302741,-78.800468234751,-78.7121217915529,
-78.6203244584689,-78.5320803365628,-78.4438496506267,-78.3556110319029,
-78.2673431110545,-78.1789748104133,-78.0905469992525,-78.0019888631497,
-77.9777431268809,-77.8891909748013,-77.8007535792782,-77.7124071360799,
-77.620609802996,-77.5323656810899,-77.4441349951538,-77.3558963764299,
-77.267628455582,-77.1792601549407,-77.0908323437798,-77.0022742076771,
-76.9780284714081,-76.8894763193284,-76.8010389238053,-76.7126924806068,
-76.6208951475229,-76.5326510256168,-76.4444203396807,-76.3561817209568,
-76.2679138001086,-76.1795454994673,-76.0911176883063,-76.0025595522034,
-75.9783138159353,-75.8897616638556,-75.8013242683325,-75.7129778251343,
-75.6211804920503,-75.5329363701443,-75.444705684208,-75.3564670654841,
-75.2681991446358,-75.1798308439944,-75.0914030328337,-75.0028448967308,
-74.9785991604624,-74.8900470083828,-74.8016096128595,-74.7132631696616,
-74.6214658365776,-74.5332217146715,-74.4449910287354,-74.3567524100117,
-74.2684844891637,-74.1801161885225,-74.0916883773617,-74.0031302412588,
-73.9788845049896,-73.8914861121851,-73.8042275676723,-73.7170488426747,
-73.6299274350949,-73.5428409004767,-73.4557374324535,-73.3686283582785,
-73.2814410301796,-73.2077874191697),.UNSPECIFIED.);
#467=B_SPLINE_CURVE_WITH_KNOTS('',3,(#68381,#68382,#68383,#68384,#68385,
#68386,#68387,#68388,#68389,#68390,#68391),.UNSPECIFIED.,.F.,.F.,(4,1,1,
1,1,1,1,1,4),(-73.2077874191697,-72.9791698495167,-71.9794551940439,-70.9797405385711,
-69.9800258830982,-68.9803112276254,-67.9805965721526,-66.9808819166797,
-66.9246021119901),.UNSPECIFIED.);
#468=B_SPLINE_CURVE_WITH_KNOTS('',3,(#68393,#68394,#68395,#68396,#68397,
#68398,#68399,#68400,#68401,#68402),.UNSPECIFIED.,.F.,.F.,(4,1,1,1,1,1,
1,4),(-66.9246021119901,-65.9811672612069,-64.9814526057341,-63.9817379502612,
-62.9820232947884,-61.9823086393156,-60.9825939838428,-60.6414242977388),
 .UNSPECIFIED.);
#469=B_SPLINE_CURVE_WITH_KNOTS('',3,(#68404,#68405,#68406,#68407,#68408,
#68409,#68410,#68411,#68412,#68413,#68414,#68415,#68416,#68417,#68418,#68419,
#68420,#68421,#68422,#68423,#68424,#68425,#68426,#68427,#68428,#68429,#68430,
#68431,#68432,#68433,#68434,#68435,#68436,#68437,#68438,#68439,#68440,#68441,
#68442,#68443,#68444,#68445,#68446,#68447,#68448,#68449,#68450,#68451,#68452,
#68453,#68454,#68455,#68456,#68457,#68458,#68459,#68460,#68461,#68462,#68463,
#68464,#68465,#68466,#68467,#68468,#68469,#68470,#68471,#68472,#68473,#68474,
#68475,#68476,#68477,#68478,#68479,#68480,#68481,#68482,#68483,#68484,#68485,
#68486,#68487,#68488,#68489,#68490,#68491,#68492,#68493,#68494,#68495,#68496,
#68497,#68498,#68499,#68500,#68501,#68502,#68503,#68504,#68505,#68506,#68507,
#68508,#68509,#68510,#68511,#68512,#68513,#68514,#68515,#68516,#68517,#68518,
#68519,#68520,#68521,#68522,#68523,#68524,#68525,#68526,#68527,#68528,#68529,
#68530,#68531,#68532,#68533,#68534,#68535,#68536,#68537,#68538,#68539,#68540,
#68541,#68542,#68543,#68544,#68545,#68546,#68547,#68548,#68549,#68550,#68551,
#68552,#68553,#68554,#68555,#68556,#68557,#68558,#68559,#68560,#68561,#68562,
#68563,#68564,#68565,#68566,#68567,#68568,#68569,#68570,#68571,#68572,#68573,
#68574,#68575,#68576,#68577,#68578,#68579,#68580,#68581,#68582,#68583,#68584,
#68585,#68586,#68587,#68588,#68589,#68590,#68591,#68592,#68593,#68594,#68595,
#68596,#68597,#68598,#68599,#68600,#68601,#68602,#68603,#68604,#68605,#68606,
#68607,#68608,#68609,#68610,#68611,#68612,#68613,#68614,#68615,#68616,#68617,
#68618,#68619,#68620,#68621,#68622,#68623,#68624,#68625,#68626,#68627,#68628,
#68629),.UNSPECIFIED.,.F.,.F.,(4,3,3,3,3,3,3,3,3,3,3,3,3,3,3,3,3,3,3,3,
3,3,3,3,3,3,3,3,3,3,3,3,3,3,3,3,3,3,3,3,3,3,3,3,3,3,3,3,3,3,3,3,3,3,3,3,
3,3,3,3,3,3,3,3,3,3,3,3,3,3,3,3,3,3,3,4),(-60.6414168048105,-60.5531164885272,
-60.4648265653877,-60.3765258343915,-60.2881930918611,-60.1997525210904,
-60.1112505357928,-60.0226065066029,-59.9828793283699,-59.8943271762903,
-59.8058897807671,-59.717543337569,-59.625746004485,-59.5375018825789,-59.4492711966428,
-59.3610325779189,-59.272764657071,-59.1843963564296,-59.0959685452685,
-59.0074104091656,-58.9831646728971,-58.8946125208176,-58.8061751252944,
-58.7178286820963,-58.6260313490123,-58.5377872271062,-58.4495565411702,
-58.3613179224462,-58.2730500015979,-58.1846817009566,-58.0962538897957,
-58.007695753693,-57.9834500174243,-57.8948978653448,-57.8064604698214,
-57.7181140266232,-57.6263166935392,-57.5380725716331,-57.449841885697,
-57.3616032669731,-57.2733353461248,-57.1849670454835,-57.0965392343224,
-57.0079810982195,-56.9837353619514,-56.8951832098719,-56.8067458143486,
-56.7183993711503,-56.6266020380664,-56.5383579161603,-56.4501272302242,
-56.3618886115005,-56.2736206906521,-56.1852523900108,-56.0968245788499,
-56.008266442747,-55.9840207064786,-55.8954685543989,-55.807031158876,-55.7186847156778,
-55.6268873825938,-55.5386432606877,-55.4504125747516,-55.3621739560279,
-55.273906035179,-55.1855377345377,-55.0971099233766,-55.008551787274,-54.9843060510058,
-54.8950533954186,-54.8059198068906,-54.71688469093,-54.6272213926052,-54.5383253255974,
-54.4482784116142,-54.3582314976309),.UNSPECIFIED.);
#470=B_SPLINE_CURVE_WITH_KNOTS('',3,(#68631,#68632,#68633,#68634,#68635,
#68636,#68637,#68638,#68639,#68640),.UNSPECIFIED.,.F.,.F.,(4,1,1,1,1,1,
1,4),(-54.3582238422873,-53.9845913955329,-52.9848767400601,-51.9851620845873,
-50.9854474291144,-49.9857327736416,-48.9860181181688,-48.0750549567666),
 .UNSPECIFIED.);
#471=B_SPLINE_CURVE_WITH_KNOTS('',3,(#68642,#68643,#68644,#68645,#68646,
#68647,#68648,#68649,#68650,#68651,#68652,#68653,#68654,#68655,#68656,#68657,
#68658,#68659,#68660,#68661,#68662,#68663,#68664,#68665,#68666,#68667,#68668,
#68669,#68670,#68671,#68672,#68673,#68674,#68675,#68676,#68677,#68678,#68679,
#68680,#68681,#68682,#68683,#68684,#68685,#68686,#68687,#68688,#68689,#68690,
#68691,#68692,#68693,#68694,#68695,#68696,#68697,#68698,#68699,#68700,#68701,
#68702,#68703,#68704,#68705,#68706,#68707,#68708,#68709,#68710,#68711,#68712,
#68713,#68714,#68715,#68716,#68717,#68718,#68719,#68720,#68721,#68722,#68723,
#68724,#68725,#68726,#68727,#68728,#68729,#68730,#68731,#68732,#68733,#68734,
#68735,#68736,#68737,#68738,#68739,#68740,#68741,#68742,#68743,#68744,#68745,
#68746,#68747,#68748,#68749,#68750,#68751,#68752,#68753,#68754,#68755,#68756,
#68757,#68758,#68759,#68760,#68761,#68762,#68763,#68764,#68765,#68766,#68767,
#68768,#68769,#68770,#68771,#68772,#68773,#68774,#68775,#68776,#68777,#68778,
#68779,#68780,#68781,#68782,#68783,#68784,#68785,#68786,#68787,#68788,#68789,
#68790,#68791,#68792,#68793,#68794,#68795,#68796,#68797,#68798,#68799,#68800,
#68801,#68802,#68803,#68804,#68805,#68806,#68807,#68808,#68809,#68810,#68811,
#68812,#68813,#68814,#68815,#68816,#68817,#68818,#68819,#68820,#68821,#68822,
#68823,#68824,#68825,#68826,#68827,#68828,#68829,#68830,#68831,#68832,#68833,
#68834,#68835,#68836,#68837,#68838,#68839,#68840,#68841,#68842,#68843,#68844,
#68845,#68846,#68847,#68848,#68849,#68850,#68851,#68852,#68853,#68854,#68855,
#68856,#68857,#68858,#68859,#68860,#68861,#68862,#68863,#68864,#68865,#68866,
#68867),.UNSPECIFIED.,.F.,.F.,(4,3,3,3,3,3,3,3,3,3,3,3,3,3,3,3,3,3,3,3,
3,3,3,3,3,3,3,3,3,3,3,3,3,3,3,3,3,3,3,3,3,3,3,3,3,3,3,3,3,3,3,3,3,3,3,3,
3,3,3,3,3,3,3,3,3,3,3,3,3,3,3,3,3,3,3,4),(-48.0750461904513,-47.9863034626959,
-47.8977513106161,-47.8093139150928,-47.7209674718944,-47.6291701388105,
-47.5409260169042,-47.4526953309678,-47.3644567122437,-47.2761887913952,
-47.1878204907537,-47.0993926795925,-47.0108345434895,-46.9865888072231,
-46.8980366551436,-46.8095992596205,-46.7212528164225,-46.6294554833385,
-46.5412113614325,-46.4529806754964,-46.3647420567726,-46.2764741359245,
-46.1881058352832,-46.0996780241223,-46.0111198880196,-45.9868741517503,
-45.8983219996707,-45.8098846041475,-45.7215381609494,-45.6297408278654,
-45.5414967059593,-45.4532660200232,-45.3650274012992,-45.2767594804509,
-45.1883911798096,-45.0999633686486,-45.0114052325458,-44.9871594962774,
-44.8986073441978,-44.8101699486746,-44.7218235054764,-44.6300261723924,
-44.5417820504863,-44.4535513645502,-44.3653127458263,-44.277044824978,
-44.1886765243367,-44.1002487131756,-44.0116905770728,-43.9874448408046,
-43.898892688725,-43.8104552932019,-43.7221088500039,-43.6303115169199,
-43.5420673950138,-43.4538367090777,-43.3655980903539,-43.2773301695055,
-43.1889618688643,-43.1005340577032,-43.0119759216005,-42.9877301853318,
-42.8991780332522,-42.810740637729,-42.7223941945309,-42.6305968614469,
-42.5423527395408,-42.4541220536047,-42.3658834348808,-42.2776155140324,
-42.1892472133912,-42.1008194022302,-42.0122612661274,-41.9880155298589,
-41.8596383787935,-41.7918608832717),.UNSPECIFIED.);
#472=B_SPLINE_CURVE_WITH_KNOTS('',3,(#68869,#68870,#68871,#68872,#68873,
#68874,#68875,#68876,#68877,#68878),.UNSPECIFIED.,.F.,.F.,(4,1,1,1,1,1,
1,4),(-41.7918572412641,-40.9883008743861,-39.9885862189133,-38.9888715634405,
-37.9891569079676,-36.9894422524948,-35.989727597022,-35.5086755760922),
 .UNSPECIFIED.);
#473=B_SPLINE_CURVE_WITH_KNOTS('',3,(#68880,#68881,#68882,#68883,#68884,
#68885,#68886,#68887,#68888,#68889),.UNSPECIFIED.,.F.,.F.,(4,1,1,1,1,1,
1,4),(-35.5086755760922,-34.9900129415491,-33.9902982860763,-32.9905836306035,
-31.9908689751306,-30.9911543196578,-29.991439664185,-29.2254902689126),
 .UNSPECIFIED.);
#474=B_SPLINE_CURVE_WITH_KNOTS('',3,(#68891,#68892,#68893,#68894,#68895,
#68896,#68897,#68898,#68899,#68900,#68901),.UNSPECIFIED.,.F.,.F.,(4,1,1,
1,1,1,1,1,4),(-29.2254902689126,-28.9917250087121,-27.9920103532393,-26.9922956977665,
-25.9925810422936,-24.9928663868208,-23.993151731348,-22.9934370758751,
-22.942304961733),.UNSPECIFIED.);
#475=B_SPLINE_CURVE_WITH_KNOTS('',3,(#68903,#68904,#68905,#68906,#68907,
#68908,#68909,#68910,#68911,#68912),.UNSPECIFIED.,.F.,.F.,(4,1,1,1,1,1,
1,4),(-22.942304961733,-21.9937224204023,-20.9940077649295,-19.9942931094566,
-18.9945784539838,-17.994863798511,-16.9951491430381,-16.6591270207278),
 .UNSPECIFIED.);
#476=B_SPLINE_CURVE_WITH_KNOTS('',3,(#68914,#68915,#68916,#68917,#68918,
#68919,#68920,#68921,#68922,#68923,#68924,#68925,#68926,#68927,#68928,#68929,
#68930,#68931,#68932,#68933,#68934,#68935,#68936,#68937,#68938,#68939,#68940,
#68941,#68942,#68943,#68944,#68945,#68946,#68947,#68948,#68949,#68950,#68951,
#68952,#68953,#68954,#68955,#68956,#68957,#68958,#68959,#68960,#68961,#68962,
#68963,#68964,#68965,#68966,#68967,#68968,#68969,#68970,#68971,#68972,#68973,
#68974,#68975,#68976,#68977,#68978,#68979,#68980,#68981,#68982,#68983,#68984,
#68985,#68986,#68987,#68988,#68989,#68990,#68991,#68992,#68993,#68994,#68995,
#68996,#68997,#68998,#68999,#69000,#69001,#69002,#69003,#69004,#69005,#69006,
#69007,#69008,#69009,#69010,#69011,#69012,#69013,#69014,#69015,#69016,#69017,
#69018,#69019,#69020,#69021,#69022,#69023,#69024,#69025,#69026,#69027,#69028,
#69029,#69030,#69031,#69032,#69033,#69034,#69035,#69036,#69037,#69038,#69039,
#69040,#69041,#69042,#69043,#69044,#69045,#69046,#69047,#69048,#69049,#69050,
#69051,#69052,#69053,#69054,#69055,#69056,#69057,#69058,#69059,#69060,#69061,
#69062,#69063,#69064,#69065,#69066,#69067,#69068,#69069,#69070,#69071,#69072,
#69073,#69074,#69075,#69076,#69077,#69078,#69079,#69080,#69081,#69082,#69083,
#69084,#69085,#69086,#69087,#69088,#69089,#69090,#69091,#69092,#69093,#69094,
#69095,#69096,#69097,#69098,#69099,#69100,#69101,#69102,#69103,#69104,#69105,
#69106,#69107,#69108,#69109,#69110,#69111,#69112,#69113,#69114,#69115,#69116,
#69117,#69118,#69119,#69120,#69121,#69122,#69123,#69124,#69125,#69126,#69127,
#69128,#69129,#69130,#69131,#69132,#69133,#69134,#69135,#69136,#69137,#69138,
#69139),.UNSPECIFIED.,.F.,.F.,(4,3,3,3,3,3,3,3,3,3,3,3,3,3,3,3,3,3,3,3,
3,3,3,3,3,3,3,3,3,3,3,3,3,3,3,3,3,3,3,3,3,3,3,3,3,3,3,3,3,3,3,3,3,3,3,3,
3,3,3,3,3,3,3,3,3,3,3,3,3,3,3,3,3,3,3,4),(-16.6591196545534,-16.5708987836911,
-16.4826909463111,-16.39447483713,-16.3062291499716,-16.2178775403357,-16.1294664880442,
-16.0409125071688,-15.9954344875653,-15.9068823127741,-15.8184448949747,
-15.7300984299549,-15.6383011052221,-15.55005696275,-15.4618262567426,-15.3735876184608,
-15.2853196785869,-15.1969513597993,-15.1085235309808,-15.0199653780704,
-14.9957198320925,-14.9071675077305,-14.8187299390432,-14.7303833220088,
-14.6385860538351,-14.5503417575066,-14.4621108972267,-14.3738721044216,
-14.2856040099394,-14.1972355372029,-14.1088075546291,-14.0202492494465,
-13.9960051766197,-13.9074534571886,-13.819016494562,-13.7306704840109,
-13.6388729886529,-13.5506292961144,-13.4623990376217,-13.3741608439751,
-13.2858933453935,-13.1975254607428,-13.1090980624374,-13.020540331398,
-12.9962905211468,-12.9077381001238,-12.8193004382952,-12.7309537316963,
-12.6391564984435,-12.5509121219219,-12.4626811850177,-12.3744423192198,
-12.2861741554417,-12.1978056191965,-12.1093775763988,-12.0208192162486,
-11.996575865674,-11.908022720017,-11.8195843246472,-11.7312368765609,-11.639439918266,
-11.5511947852311,-11.4629630875814,-11.3747234576318,-11.2864545271203,
-11.1980852242406,-11.1096564139226,-11.021097290955,-10.9968612102012,
-10.9075004241338,-10.8182598130855,-10.7291189426381,-10.640067321383,
-10.5510692741881,-10.4620920011923,-10.3759343473738),.UNSPECIFIED.);
#477=B_SPLINE_CURVE_WITH_KNOTS('',3,(#69140,#69141,#69142,#69143,#69144,
#69145,#69146,#69147,#69148,#69149),.UNSPECIFIED.,.F.,.F.,(4,1,1,1,1,1,
1,4),(-10.3759267640895,-9.99714655472832,-8.99743189925549,-7.99771724378266,
-6.99800258830983,-5.99828793283699,-4.99857327736416,-4.0927579448374),
 .UNSPECIFIED.);
#478=B_SPLINE_CURVE_WITH_KNOTS('',3,(#69152,#69153,#69154,#69155,#69156,
#69157,#69158,#69159,#69160,#69161,#69162,#69163,#69164,#69165,#69166,#69167,
#69168,#69169,#69170,#69171,#69172,#69173,#69174,#69175,#69176,#69177,#69178,
#69179,#69180,#69181,#69182,#69183,#69184,#69185,#69186,#69187,#69188,#69189,
#69190,#69191,#69192,#69193,#69194,#69195,#69196,#69197,#69198,#69199,#69200,
#69201,#69202,#69203,#69204,#69205,#69206,#69207,#69208,#69209,#69210,#69211,
#69212,#69213,#69214,#69215,#69216,#69217,#69218,#69219,#69220,#69221,#69222,
#69223,#69224,#69225,#69226,#69227,#69228,#69229,#69230,#69231,#69232,#69233,
#69234,#69235,#69236,#69237,#69238,#69239,#69240,#69241,#69242,#69243,#69244,
#69245,#69246,#69247,#69248,#69249,#69250,#69251,#69252,#69253,#69254,#69255,
#69256,#69257,#69258,#69259,#69260,#69261,#69262,#69263,#69264,#69265,#69266,
#69267,#69268,#69269,#69270,#69271,#69272,#69273,#69274,#69275,#69276,#69277,
#69278,#69279,#69280,#69281,#69282,#69283,#69284,#69285,#69286,#69287,#69288,
#69289,#69290,#69291,#69292,#69293,#69294,#69295,#69296,#69297,#69298,#69299,
#69300,#69301,#69302,#69303,#69304,#69305,#69306,#69307,#69308,#69309,#69310,
#69311,#69312,#69313,#69314,#69315,#69316,#69317,#69318,#69319,#69320,#69321,
#69322,#69323,#69324,#69325),.UNSPECIFIED.,.F.,.F.,(4,2,2,2,2,2,2,2,2,2,
2,2,2,2,2,2,2,2,2,2,2,2,2,2,2,2,2,2,2,2,2,2,2,2,2,2,2,2,2,2,2,2,2,2,2,2,
2,2,2,2,2,2,2,2,2,2,2,2,2,2,2,2,2,2,2,2,2,2,2,2,2,2,2,2,2,2,2,2,2,2,2,2,
2,2,2,2,4),(0.00584818159483936,0.0833145403087904,0.119798541190528,0.141538318830421,
0.144170087014775,0.14547429476973,0.14640642714708,0.147387815864638,0.148759121781876,
0.151564746211207,0.17973329450901,0.228089013742081,0.273503294053368,
0.297374946185057,0.300084718010428,0.302053797000991,0.302879679694602,
0.303424952652158,0.304011448637213,0.30484292497825,0.306844998348911,
0.338167487368042,0.363754212317079,0.411681980848662,0.440764683950415,
0.459769203371667,0.462300484273235,0.463574433775327,0.464492643053152,
0.465466495291672,0.466838865743283,0.469683937477996,0.500400276153216,
0.501264789422534,0.574394376789672,0.603104757062347,0.6218330455912,0.624956632985009,
0.625928445141098,0.62653096481541,0.627084504034372,0.627803388533153,
0.629272470720125,0.639037815668281,0.693580567889972,0.753391160794976,
0.770644744200646,0.78401986068556,0.78631853951607,0.787534200465984,0.788531406216088,
0.789535684326634,0.791379603931896,0.797287122663885,0.914564704302383,
0.938494556661125,0.94800309566758,0.949366136088689,0.950050469151676,
0.950598288780364,0.951218819934483,0.952241022135733,0.955622252115452,
1.01353206910293,1.07220338839884,1.09604162916153,1.10812992399944,1.11038272606639,
1.11159650679142,1.11259449467071,1.11361659302962,1.11551456922664,1.12176740763345,
1.22748453082085,1.25144601047151,1.2685531134962,1.27151244538824,1.27246729746659,
1.27306771867178,1.27362609079136,1.2743617612658,1.2758957178046,1.28697388512726,
1.28934319240167,1.29049736874123,1.37002912032471,1.37016181069821),
 .UNSPECIFIED.);
#479=B_SPLINE_CURVE_WITH_KNOTS('',3,(#69329,#69330,#69331,#69332,#69333,
#69334,#69335,#69336,#69337,#69338,#69339,#69340,#69341,#69342,#69343,#69344,
#69345,#69346,#69347,#69348,#69349,#69350,#69351,#69352,#69353,#69354,#69355,
#69356,#69357,#69358,#69359),.UNSPECIFIED.,.F.,.F.,(4,3,3,3,3,3,3,3,3,3,
4),(537.212343764025,537.307206720962,537.401923457098,537.497120543768,
537.591603148533,537.686022182108,537.780399718832,537.876174826739,537.970560964813,
538.067030557636,538.16350015046),.UNSPECIFIED.);
#480=B_SPLINE_CURVE_WITH_KNOTS('',3,(#69360,#69361,#69362,#69363,#69364,
#69365,#69366,#69367,#69368,#69369,#69370,#69371,#69372,#69373,#69374,#69375,
#69376,#69377,#69378,#69379,#69380,#69381,#69382,#69383,#69384,#69385,#69386,
#69387,#69388,#69389,#69390,#69391,#69392,#69393,#69394,#69395,#69396,#69397,
#69398,#69399,#69400,#69401,#69402,#69403,#69404,#69405,#69406,#69407,#69408,
#69409,#69410,#69411,#69412,#69413,#69414,#69415,#69416,#69417,#69418,#69419,
#69420,#69421,#69422,#69423,#69424,#69425,#69426,#69427,#69428,#69429),
 .UNSPECIFIED.,.F.,.F.,(4,3,3,3,3,3,3,3,3,3,3,3,3,3,3,3,3,3,3,3,3,3,3,4),
(535.166163310789,535.259377415355,535.352468125424,535.44546285116,535.538392707924,
535.631289207834,535.724176983089,535.817080652029,535.910084313234,536.003140721908,
536.096351253059,536.164070839515,536.256098879168,536.348000065887,536.439803195721,
536.531542963888,536.623250393304,536.714951321204,536.806671573945,536.898504795489,
536.990395572781,537.082462154414,537.163785494987,537.212343763855),
 .UNSPECIFIED.);
#481=B_SPLINE_CURVE_WITH_KNOTS('',3,(#71562,#71563,#71564,#71565,#71566,
#71567,#71568,#71569,#71570,#71571,#71572,#71573,#71574,#71575,#71576,#71577,
#71578,#71579,#71580,#71581,#71582,#71583,#71584,#71585,#71586,#71587,#71588,
#71589,#71590,#71591,#71592,#71593,#71594,#71595,#71596,#71597,#71598,#71599,
#71600,#71601,#71602,#71603,#71604,#71605,#71606,#71607,#71608,#71609,#71610,
#71611,#71612,#71613,#71614,#71615,#71616,#71617,#71618,#71619,#71620,#71621,
#71622,#71623,#71624,#71625,#71626,#71627,#71628,#71629,#71630,#71631,#71632,
#71633,#71634,#71635,#71636,#71637,#71638,#71639,#71640,#71641,#71642,#71643,
#71644,#71645,#71646,#71647,#71648,#71649,#71650,#71651,#71652,#71653,#71654,
#71655,#71656,#71657,#71658),.UNSPECIFIED.,.F.,.F.,(4,3,3,3,3,3,3,3,3,3,
3,3,3,3,3,3,3,3,3,3,3,3,3,3,3,3,3,3,3,3,3,3,4),(0.,0.024358377757175,0.0606004463391366,
0.0979427454018428,0.135285044464549,0.147496336806586,0.153993564102934,
0.189847058097303,0.225532572426869,0.260944091043929,0.278511116143725,
0.288145210622836,0.295840256144695,0.300686689054012,0.335177193005298,
0.368740608710732,0.4014802918423,0.435215231454813,0.439494929020506,0.47314786573973,
0.507110508987375,0.540835061830413,0.566063267316088,0.571536025515506,
0.576790817926267,0.610135744437123,0.643480670947979,0.652892754403838,
0.658607915903714,0.664640539756856,0.696454722966971,0.727403443102524,
0.744397949170609),.UNSPECIFIED.);
#482=B_SPLINE_CURVE_WITH_KNOTS('',3,(#71659,#71660,#71661,#71662,#71663,
#71664,#71665,#71666,#71667,#71668,#71669,#71670,#71671,#71672,#71673,#71674,
#71675,#71676,#71677,#71678,#71679,#71680,#71681,#71682,#71683,#71684,#71685,
#71686,#71687,#71688,#71689,#71690,#71691,#71692,#71693,#71694,#71695,#71696,
#71697,#71698,#71699,#71700,#71701,#71702,#71703,#71704,#71705,#71706,#71707,
#71708,#71709,#71710,#71711,#71712,#71713,#71714,#71715,#71716,#71717,#71718,
#71719,#71720,#71721,#71722,#71723,#71724,#71725,#71726,#71727,#71728,#71729,
#71730,#71731,#71732,#71733,#71734,#71735,#71736,#71737,#71738,#71739,#71740,
#71741,#71742,#71743,#71744,#71745,#71746,#71747,#71748,#71749,#71750,#71751,
#71752),.UNSPECIFIED.,.F.,.F.,(4,3,3,3,3,3,3,3,3,3,3,3,3,3,3,3,3,3,3,3,
3,3,3,3,3,3,3,3,3,3,3,4),(0.,0.0201115232403622,0.0509103820036684,0.0827015579379697,
0.114480781419795,0.125233641024824,0.130996774529478,0.163645515795945,
0.196840351068161,0.230356207922839,0.247143998849504,0.25945135865808,
0.263664864268182,0.298048672203931,0.332324436198921,0.364116142924617,
0.387688307017233,0.395015510154993,0.401768807630668,0.435672330857666,
0.47020591900154,0.50544680147227,0.534532831369196,0.540976992820617,0.546669086825655,
0.582618106602,0.618832117278038,0.635189667272764,0.64457122033922,0.681413970877714,
0.717779744788314,0.741270768406475),.UNSPECIFIED.);
#483=B_SPLINE_CURVE_WITH_KNOTS('',3,(#73886,#73887,#73888,#73889,#73890,
#73891,#73892,#73893,#73894,#73895,#73896,#73897,#73898,#73899,#73900,#73901,
#73902,#73903,#73904,#73905,#73906,#73907,#73908,#73909,#73910,#73911,#73912,
#73913,#73914,#73915,#73916,#73917,#73918,#73919,#73920,#73921,#73922,#73923,
#73924,#73925,#73926,#73927,#73928,#73929,#73930,#73931,#73932,#73933,#73934,
#73935,#73936,#73937,#73938,#73939,#73940,#73941,#73942,#73943,#73944,#73945,
#73946,#73947,#73948,#73949,#73950,#73951,#73952,#73953,#73954,#73955,#73956,
#73957,#73958,#73959,#73960,#73961,#73962,#73963,#73964,#73965,#73966,#73967,
#73968,#73969,#73970,#73971,#73972,#73973,#73974,#73975,#73976,#73977,#73978,
#73979),.UNSPECIFIED.,.F.,.F.,(4,3,3,3,3,3,3,3,3,3,3,3,3,3,3,3,3,3,3,3,
3,3,3,3,3,3,3,3,3,3,3,4),(0.,0.0201115232402943,0.0509103821130776,0.0827015580720687,
0.114480781418801,0.125233641028996,0.130996774690604,0.163535076161932,
0.196984384449669,0.230433692737407,0.247143999010811,0.259451358570654,
0.265189960467916,0.299585032738881,0.333849079024935,0.364116142924638,
0.387688307017256,0.39501551015294,0.401768807899556,0.435672331184667,
0.470205918898849,0.505446801388904,0.534532831632145,0.540976995161682,
0.546669087389317,0.582793053609079,0.618874393635674,0.635189668141087,
0.644571220279675,0.681413970914885,0.717779744663936,0.741270768406529),
 .UNSPECIFIED.);
#484=B_SPLINE_CURVE_WITH_KNOTS('',3,(#73980,#73981,#73982,#73983),
 .UNSPECIFIED.,.F.,.F.,(4,4),(0.,0.0151734474062035),.UNSPECIFIED.);
#485=B_SPLINE_CURVE_WITH_KNOTS('',3,(#73984,#73985,#73986,#73987,#73988,
#73989,#73990,#73991,#73992,#73993,#73994,#73995,#73996,#73997,#73998,#73999,
#74000,#74001,#74002,#74003,#74004,#74005,#74006,#74007,#74008,#74009,#74010,
#74011,#74012,#74013,#74014,#74015,#74016,#74017,#74018,#74019,#74020,#74021,
#74022,#74023,#74024,#74025,#74026,#74027,#74028,#74029,#74030,#74031,#74032,
#74033,#74034,#74035,#74036,#74037,#74038,#74039,#74040,#74041,#74042,#74043,
#74044,#74045,#74046,#74047,#74048,#74049,#74050,#74051,#74052,#74053,#74054,
#74055,#74056,#74057,#74058,#74059,#74060,#74061,#74062,#74063,#74064,#74065,
#74066,#74067,#74068,#74069,#74070,#74071,#74072,#74073,#74074,#74075,#74076,
#74077,#74078,#74079,#74080),.UNSPECIFIED.,.F.,.F.,(4,3,3,3,3,3,3,3,3,3,
3,3,3,3,3,3,3,3,3,3,3,3,3,3,3,3,3,3,3,3,3,3,4),(0.,0.0243583777572955,0.0606004463128303,
0.0979427454027436,0.135285044492657,0.147496336813618,0.153993563998701,
0.189887631727371,0.225706497374811,0.260756281969611,0.288145210372972,
0.295840255200718,0.300686688874331,0.335177192775901,0.368740608421313,
0.401480291842367,0.422912645425388,0.435215231449938,0.439494929180684,
0.473147865916593,0.50711050909266,0.540835061994793,0.566063267486325,
0.571536022966052,0.576790817150764,0.609861602079571,0.642320376686977,
0.652892753239362,0.658607918910948,0.664640540296814,0.69645472327343,
0.727403443285381,0.744397949170614),.UNSPECIFIED.);
#489=SHAPE_REPRESENTATION_RELATIONSHIP('SRR','None',#74131,#493);
#493=ADVANCED_BREP_SHAPE_REPRESENTATION('',(#501),#74102);
#497=STYLED_ITEM('',(#74159),#501);
#501=MANIFOLD_SOLID_BREP('Body1',#4576);
#610=PLANE('',#4936);
#611=PLANE('',#4937);
#708=FACE_OUTER_BOUND('',#920,.T.);
#709=FACE_OUTER_BOUND('',#921,.T.);
#710=FACE_OUTER_BOUND('',#922,.T.);
#711=FACE_OUTER_BOUND('',#923,.T.);
#712=FACE_OUTER_BOUND('',#924,.T.);
#713=FACE_OUTER_BOUND('',#925,.T.);
#714=FACE_OUTER_BOUND('',#926,.T.);
#715=FACE_OUTER_BOUND('',#927,.T.);
#716=FACE_OUTER_BOUND('',#928,.T.);
#717=FACE_OUTER_BOUND('',#929,.T.);
#718=FACE_OUTER_BOUND('',#930,.T.);
#719=FACE_OUTER_BOUND('',#931,.T.);
#720=FACE_OUTER_BOUND('',#932,.T.);
#721=FACE_OUTER_BOUND('',#933,.T.);
#722=FACE_OUTER_BOUND('',#934,.T.);
#723=FACE_OUTER_BOUND('',#935,.T.);
#724=FACE_OUTER_BOUND('',#936,.T.);
#725=FACE_OUTER_BOUND('',#937,.T.);
#726=FACE_OUTER_BOUND('',#938,.T.);
#727=FACE_OUTER_BOUND('',#939,.T.);
#728=FACE_OUTER_BOUND('',#940,.T.);
#729=FACE_OUTER_BOUND('',#941,.T.);
#730=FACE_OUTER_BOUND('',#942,.T.);
#731=FACE_OUTER_BOUND('',#943,.T.);
#732=FACE_OUTER_BOUND('',#944,.T.);
#733=FACE_OUTER_BOUND('',#945,.T.);
#734=FACE_OUTER_BOUND('',#946,.T.);
#735=FACE_OUTER_BOUND('',#947,.T.);
#736=FACE_OUTER_BOUND('',#948,.T.);
#737=FACE_OUTER_BOUND('',#949,.T.);
#738=FACE_OUTER_BOUND('',#950,.T.);
#739=FACE_OUTER_BOUND('',#951,.T.);
#740=FACE_OUTER_BOUND('',#952,.T.);
#741=FACE_OUTER_BOUND('',#953,.T.);
#742=FACE_OUTER_BOUND('',#954,.T.);
#743=FACE_OUTER_BOUND('',#955,.T.);
#744=FACE_OUTER_BOUND('',#956,.T.);
#745=FACE_OUTER_BOUND('',#957,.T.);
#746=FACE_OUTER_BOUND('',#958,.T.);
#747=FACE_OUTER_BOUND('',#959,.T.);
#748=FACE_OUTER_BOUND('',#960,.T.);
#749=FACE_OUTER_BOUND('',#961,.T.);
#750=FACE_OUTER_BOUND('',#962,.T.);
#751=FACE_OUTER_BOUND('',#963,.T.);
#752=FACE_OUTER_BOUND('',#964,.T.);
#753=FACE_OUTER_BOUND('',#965,.T.);
#754=FACE_OUTER_BOUND('',#966,.T.);
#755=FACE_OUTER_BOUND('',#967,.T.);
#756=FACE_OUTER_BOUND('',#968,.T.);
#757=FACE_OUTER_BOUND('',#969,.T.);
#758=FACE_OUTER_BOUND('',#970,.T.);
#759=FACE_OUTER_BOUND('',#971,.T.);
#760=FACE_OUTER_BOUND('',#972,.T.);
#761=FACE_OUTER_BOUND('',#973,.T.);
#762=FACE_OUTER_BOUND('',#974,.T.);
#763=FACE_OUTER_BOUND('',#975,.T.);
#764=FACE_OUTER_BOUND('',#976,.T.);
#765=FACE_OUTER_BOUND('',#977,.T.);
#766=FACE_OUTER_BOUND('',#978,.T.);
#767=FACE_OUTER_BOUND('',#979,.T.);
#768=FACE_OUTER_BOUND('',#980,.T.);
#769=FACE_OUTER_BOUND('',#981,.T.);
#770=FACE_OUTER_BOUND('',#982,.T.);
#771=FACE_OUTER_BOUND('',#983,.T.);
#772=FACE_OUTER_BOUND('',#984,.T.);
#773=FACE_OUTER_BOUND('',#985,.T.);
#774=FACE_OUTER_BOUND('',#986,.T.);
#775=FACE_OUTER_BOUND('',#987,.T.);
#776=FACE_OUTER_BOUND('',#988,.T.);
#777=FACE_OUTER_BOUND('',#989,.T.);
#778=FACE_OUTER_BOUND('',#990,.T.);
#779=FACE_OUTER_BOUND('',#991,.T.);
#780=FACE_OUTER_BOUND('',#992,.T.);
#781=FACE_OUTER_BOUND('',#993,.T.);
#782=FACE_OUTER_BOUND('',#994,.T.);
#783=FACE_OUTER_BOUND('',#995,.T.);
#784=FACE_OUTER_BOUND('',#996,.T.);
#785=FACE_OUTER_BOUND('',#997,.T.);
#786=FACE_OUTER_BOUND('',#998,.T.);
#787=FACE_OUTER_BOUND('',#999,.T.);
#788=FACE_OUTER_BOUND('',#1000,.T.);
#789=FACE_OUTER_BOUND('',#1001,.T.);
#790=FACE_OUTER_BOUND('',#1002,.T.);
#791=FACE_OUTER_BOUND('',#1003,.T.);
#792=FACE_OUTER_BOUND('',#1004,.T.);
#793=FACE_OUTER_BOUND('',#1005,.T.);
#794=FACE_OUTER_BOUND('',#1006,.T.);
#795=FACE_OUTER_BOUND('',#1007,.T.);
#796=FACE_OUTER_BOUND('',#1008,.T.);
#797=FACE_OUTER_BOUND('',#1009,.T.);
#920=EDGE_LOOP('',(#3205,#3206,#3207,#3208));
#921=EDGE_LOOP('',(#3209,#3210,#3211,#3212,#3213,#3214));
#922=EDGE_LOOP('',(#3215,#3216,#3217,#3218));
#923=EDGE_LOOP('',(#3219,#3220,#3221,#3222,#3223,#3224));
#924=EDGE_LOOP('',(#3225,#3226,#3227,#3228));
#925=EDGE_LOOP('',(#3229,#3230,#3231,#3232,#3233,#3234));
#926=EDGE_LOOP('',(#3235,#3236,#3237,#3238));
#927=EDGE_LOOP('',(#3239,#3240,#3241,#3242,#3243,#3244));
#928=EDGE_LOOP('',(#3245,#3246,#3247,#3248));
#929=EDGE_LOOP('',(#3249,#3250,#3251,#3252,#3253,#3254));
#930=EDGE_LOOP('',(#3255,#3256,#3257,#3258));
#931=EDGE_LOOP('',(#3259,#3260,#3261,#3262,#3263,#3264));
#932=EDGE_LOOP('',(#3265,#3266,#3267,#3268));
#933=EDGE_LOOP('',(#3269,#3270,#3271,#3272,#3273,#3274));
#934=EDGE_LOOP('',(#3275,#3276,#3277,#3278));
#935=EDGE_LOOP('',(#3279,#3280,#3281,#3282,#3283,#3284));
#936=EDGE_LOOP('',(#3285,#3286,#3287,#3288,#3289));
#937=EDGE_LOOP('',(#3290,#3291,#3292,#3293,#3294));
#938=EDGE_LOOP('',(#3295,#3296,#3297,#3298,#3299));
#939=EDGE_LOOP('',(#3300,#3301,#3302,#3303,#3304));
#940=EDGE_LOOP('',(#3305,#3306,#3307,#3308,#3309));
#941=EDGE_LOOP('',(#3310,#3311,#3312,#3313,#3314));
#942=EDGE_LOOP('',(#3315,#3316,#3317,#3318,#3319));
#943=EDGE_LOOP('',(#3320,#3321,#3322,#3323,#3324));
#944=EDGE_LOOP('',(#3325,#3326,#3327,#3328,#3329));
#945=EDGE_LOOP('',(#3330,#3331,#3332,#3333,#3334));
#946=EDGE_LOOP('',(#3335,#3336,#3337,#3338,#3339));
#947=EDGE_LOOP('',(#3340,#3341,#3342,#3343,#3344));
#948=EDGE_LOOP('',(#3345,#3346,#3347,#3348,#3349));
#949=EDGE_LOOP('',(#3350,#3351,#3352,#3353,#3354));
#950=EDGE_LOOP('',(#3355,#3356,#3357,#3358,#3359));
#951=EDGE_LOOP('',(#3360,#3361,#3362,#3363,#3364));
#952=EDGE_LOOP('',(#3365,#3366,#3367,#3368,#3369));
#953=EDGE_LOOP('',(#3370,#3371,#3372,#3373,#3374));
#954=EDGE_LOOP('',(#3375,#3376,#3377,#3378,#3379));
#955=EDGE_LOOP('',(#3380,#3381,#3382,#3383,#3384));
#956=EDGE_LOOP('',(#3385,#3386,#3387,#3388,#3389));
#957=EDGE_LOOP('',(#3390,#3391,#3392,#3393,#3394,#3395));
#958=EDGE_LOOP('',(#3396,#3397,#3398,#3399));
#959=EDGE_LOOP('',(#3400,#3401,#3402,#3403,#3404,#3405));
#960=EDGE_LOOP('',(#3406,#3407,#3408,#3409,#3410));
#961=EDGE_LOOP('',(#3411,#3412,#3413,#3414,#3415));
#962=EDGE_LOOP('',(#3416,#3417,#3418,#3419,#3420));
#963=EDGE_LOOP('',(#3421,#3422,#3423,#3424,#3425));
#964=EDGE_LOOP('',(#3426,#3427,#3428,#3429,#3430,#3431));
#965=EDGE_LOOP('',(#3432,#3433,#3434,#3435,#3436));
#966=EDGE_LOOP('',(#3437,#3438,#3439,#3440,#3441));
#967=EDGE_LOOP('',(#3442,#3443,#3444,#3445,#3446));
#968=EDGE_LOOP('',(#3447,#3448,#3449,#3450,#3451));
#969=EDGE_LOOP('',(#3452,#3453,#3454,#3455,#3456));
#970=EDGE_LOOP('',(#3457,#3458,#3459,#3460,#3461,#3462));
#971=EDGE_LOOP('',(#3463,#3464,#3465,#3466,#3467));
#972=EDGE_LOOP('',(#3468,#3469,#3470,#3471,#3472));
#973=EDGE_LOOP('',(#3473,#3474,#3475,#3476,#3477,#3478));
#974=EDGE_LOOP('',(#3479,#3480,#3481,#3482));
#975=EDGE_LOOP('',(#3483,#3484,#3485,#3486,#3487,#3488));
#976=EDGE_LOOP('',(#3489,#3490,#3491,#3492,#3493));
#977=EDGE_LOOP('',(#3494,#3495,#3496,#3497,#3498));
#978=EDGE_LOOP('',(#3499,#3500,#3501,#3502,#3503));
#979=EDGE_LOOP('',(#3504,#3505,#3506,#3507,#3508));
#980=EDGE_LOOP('',(#3509,#3510,#3511,#3512,#3513));
#981=EDGE_LOOP('',(#3514,#3515,#3516,#3517,#3518));
#982=EDGE_LOOP('',(#3519,#3520,#3521,#3522,#3523));
#983=EDGE_LOOP('',(#3524,#3525,#3526,#3527,#3528));
#984=EDGE_LOOP('',(#3529,#3530,#3531,#3532,#3533));
#985=EDGE_LOOP('',(#3534,#3535,#3536,#3537,#3538));
#986=EDGE_LOOP('',(#3539,#3540,#3541,#3542,#3543));
#987=EDGE_LOOP('',(#3544,#3545,#3546,#3547,#3548));
#988=EDGE_LOOP('',(#3549,#3550,#3551,#3552,#3553));
#989=EDGE_LOOP('',(#3554,#3555,#3556,#3557,#3558));
#990=EDGE_LOOP('',(#3559,#3560,#3561,#3562,#3563,#3564));
#991=EDGE_LOOP('',(#3565,#3566,#3567,#3568,#3569));
#992=EDGE_LOOP('',(#3570,#3571,#3572,#3573,#3574));
#993=EDGE_LOOP('',(#3575,#3576,#3577,#3578,#3579,#3580));
#994=EDGE_LOOP('',(#3581,#3582,#3583,#3584,#3585));
#995=EDGE_LOOP('',(#3586,#3587,#3588,#3589,#3590));
#996=EDGE_LOOP('',(#3591,#3592,#3593,#3594,#3595));
#997=EDGE_LOOP('',(#3596,#3597,#3598,#3599,#3600));
#998=EDGE_LOOP('',(#3601,#3602,#3603,#3604,#3605));
#999=EDGE_LOOP('',(#3606,#3607,#3608,#3609,#3610));
#1000=EDGE_LOOP('',(#3611,#3612,#3613,#3614,#3615));
#1001=EDGE_LOOP('',(#3616,#3617,#3618,#3619,#3620,#3621));
#1002=EDGE_LOOP('',(#3622,#3623,#3624,#3625));
#1003=EDGE_LOOP('',(#3626,#3627,#3628,#3629,#3630,#3631));
#1004=EDGE_LOOP('',(#3632,#3633,#3634,#3635,#3636,#3637,#3638,#3639,#3640,
#3641,#3642,#3643,#3644,#3645,#3646,#3647,#3648,#3649,#3650,#3651,#3652,
#3653,#3654,#3655,#3656,#3657,#3658,#3659,#3660,#3661,#3662,#3663,#3664,
#3665,#3666,#3667,#3668,#3669,#3670,#3671,#3672,#3673,#3674,#3675,#3676,
#3677,#3678,#3679,#3680,#3681,#3682,#3683,#3684,#3685,#3686,#3687,#3688,
#3689,#3690,#3691,#3692,#3693,#3694,#3695,#3696,#3697,#3698,#3699,#3700,
#3701,#3702,#3703,#3704,#3705,#3706,#3707,#3708,#3709,#3710,#3711,#3712,
#3713,#3714,#3715,#3716,#3717,#3718,#3719,#3720,#3721,#3722,#3723,#3724,
#3725,#3726,#3727,#3728,#3729,#3730,#3731,#3732,#3733,#3734,#3735,#3736,
#3737,#3738,#3739,#3740,#3741,#3742,#3743,#3744,#3745,#3746,#3747,#3748,
#3749,#3750,#3751,#3752,#3753,#3754,#3755,#3756,#3757,#3758,#3759,#3760,
#3761,#3762,#3763,#3764,#3765,#3766,#3767,#3768,#3769,#3770,#3771,#3772,
#3773,#3774,#3775,#3776,#3777,#3778,#3779,#3780,#3781,#3782,#3783,#3784,
#3785,#3786,#3787,#3788,#3789,#3790,#3791,#3792,#3793,#3794,#3795,#3796,
#3797,#3798,#3799,#3800,#3801,#3802,#3803));
#1005=EDGE_LOOP('',(#3804,#3805,#3806,#3807,#3808));
#1006=EDGE_LOOP('',(#3809,#3810,#3811,#3812,#3813,#3814,#3815,#3816,#3817,
#3818,#3819,#3820,#3821,#3822,#3823,#3824,#3825,#3826,#3827,#3828,#3829,
#3830,#3831,#3832,#3833,#3834,#3835,#3836,#3837,#3838,#3839,#3840,#3841,
#3842,#3843,#3844,#3845,#3846,#3847,#3848,#3849,#3850,#3851,#3852,#3853,
#3854,#3855,#3856,#3857,#3858,#3859,#3860,#3861,#3862,#3863,#3864,#3865,
#3866,#3867,#3868,#3869,#3870,#3871,#3872,#3873,#3874,#3875,#3876,#3877,
#3878,#3879,#3880,#3881,#3882,#3883,#3884,#3885,#3886,#3887,#3888,#3889,
#3890,#3891,#3892,#3893,#3894,#3895,#3896,#3897,#3898,#3899,#3900,#3901,
#3902,#3903,#3904,#3905,#3906,#3907,#3908,#3909,#3910,#3911,#3912,#3913,
#3914,#3915,#3916,#3917,#3918,#3919,#3920,#3921,#3922,#3923,#3924,#3925,
#3926,#3927,#3928,#3929,#3930,#3931,#3932,#3933,#3934,#3935,#3936,#3937,
#3938,#3939,#3940,#3941,#3942,#3943,#3944,#3945,#3946,#3947,#3948,#3949,
#3950,#3951,#3952,#3953,#3954,#3955,#3956,#3957,#3958,#3959,#3960,#3961,
#3962,#3963,#3964,#3965,#3966,#3967,#3968,#3969,#3970,#3971,#3972,#3973,
#3974,#3975,#3976,#3977,#3978,#3979,#3980,#3981,#3982,#3983,#3984,#3985,
#3986,#3987,#3988,#3989,#3990,#3991,#3992,#3993,#3994,#3995,#3996,#3997,
#3998,#3999,#4000,#4001,#4002,#4003,#4004,#4005,#4006,#4007,#4008,#4009,
#4010,#4011,#4012,#4013,#4014,#4015,#4016,#4017,#4018,#4019,#4020,#4021,
#4022,#4023,#4024,#4025,#4026));
#1007=EDGE_LOOP('',(#4027,#4028,#4029,#4030,#4031,#4032,#4033,#4034,#4035,
#4036,#4037,#4038,#4039,#4040,#4041,#4042,#4043,#4044,#4045,#4046,#4047,
#4048,#4049,#4050,#4051,#4052,#4053,#4054,#4055,#4056,#4057,#4058,#4059,
#4060,#4061,#4062,#4063,#4064,#4065,#4066,#4067,#4068,#4069,#4070,#4071,
#4072,#4073,#4074,#4075,#4076,#4077,#4078,#4079,#4080,#4081,#4082,#4083,
#4084,#4085,#4086,#4087,#4088,#4089,#4090,#4091,#4092,#4093,#4094,#4095,
#4096,#4097,#4098,#4099,#4100,#4101,#4102,#4103,#4104,#4105,#4106,#4107,
#4108,#4109,#4110,#4111,#4112,#4113,#4114,#4115,#4116,#4117,#4118,#4119,
#4120,#4121,#4122,#4123,#4124,#4125,#4126,#4127,#4128,#4129,#4130,#4131,
#4132,#4133,#4134,#4135,#4136,#4137,#4138,#4139,#4140,#4141,#4142,#4143,
#4144,#4145,#4146,#4147,#4148,#4149,#4150,#4151,#4152,#4153,#4154,#4155,
#4156,#4157,#4158,#4159,#4160,#4161,#4162,#4163,#4164,#4165,#4166,#4167,
#4168,#4169,#4170,#4171,#4172,#4173,#4174,#4175,#4176,#4177,#4178,#4179,
#4180,#4181,#4182,#4183,#4184,#4185,#4186,#4187,#4188,#4189,#4190,#4191,
#4192,#4193,#4194,#4195,#4196,#4197,#4198,#4199,#4200,#4201,#4202,#4203,
#4204,#4205,#4206,#4207,#4208,#4209,#4210,#4211,#4212,#4213,#4214,#4215,
#4216,#4217,#4218,#4219,#4220,#4221,#4222,#4223,#4224,#4225,#4226,#4227,
#4228,#4229,#4230,#4231,#4232,#4233,#4234,#4235,#4236,#4237,#4238,#4239,
#4240,#4241,#4242,#4243,#4244,#4245));
#1008=EDGE_LOOP('',(#4246,#4247,#4248,#4249,#4250));
#1009=EDGE_LOOP('',(#4251,#4252,#4253,#4254));
#1104=LINE('',#6227,#1282);
#1105=LINE('',#6416,#1283);
#1106=LINE('',#6989,#1284);
#1107=LINE('',#7567,#1285);
#1108=LINE('',#8159,#1286);
#1109=LINE('',#8711,#1287);
#1110=LINE('',#9319,#1288);
#1111=LINE('',#9901,#1289);
#1112=LINE('',#10517,#1290);
#1113=LINE('',#11063,#1291);
#1114=LINE('',#11697,#1292);
#1115=LINE('',#12261,#1293);
#1116=LINE('',#12875,#1294);
#1117=LINE('',#13439,#1295);
#1118=LINE('',#14047,#1296);
#1119=LINE('',#14615,#1297);
#1120=LINE('',#15207,#1298);
#1121=LINE('',#15798,#1299);
#1122=LINE('',#16429,#1300);
#1123=LINE('',#17070,#1301);
#1124=LINE('',#17613,#1302);
#1125=LINE('',#18324,#1303);
#1126=LINE('',#18929,#1304);
#1127=LINE('',#19652,#1305);
#1128=LINE('',#20219,#1306);
#1129=LINE('',#20836,#1307);
#1130=LINE('',#21423,#1308);
#1131=LINE('',#22026,#1309);
#1132=LINE('',#22619,#1310);
#1133=LINE('',#23222,#1311);
#1134=LINE('',#23827,#1312);
#1135=LINE('',#24392,#1313);
#1136=LINE('',#24967,#1314);
#1137=LINE('',#25560,#1315);
#1138=LINE('',#26111,#1316);
#1139=LINE('',#26700,#1317);
#1140=LINE('',#27311,#1318);
#1141=LINE('',#27902,#1319);
#1142=LINE('',#28488,#1320);
#1143=LINE('',#29136,#1321);
#1144=LINE('',#29644,#1322);
#1145=LINE('',#30202,#1323);
#1146=LINE('',#30813,#1324);
#1147=LINE('',#31392,#1325);
#1148=LINE('',#31945,#1326);
#1149=LINE('',#32463,#1327);
#1150=LINE('',#32990,#1328);
#1151=LINE('',#33615,#1329);
#1152=LINE('',#34196,#1330);
#1153=LINE('',#34863,#1331);
#1154=LINE('',#35396,#1332);
#1155=LINE('',#35886,#1333);
#1156=LINE('',#36445,#1334);
#1157=LINE('',#37032,#1335);
#1158=LINE('',#37622,#1336);
#1159=LINE('',#38172,#1337);
#1160=LINE('',#38700,#1338);
#1161=LINE('',#39229,#1339);
#1162=LINE('',#39816,#1340);
#1163=LINE('',#40425,#1341);
#1164=LINE('',#41062,#1342);
#1165=LINE('',#41669,#1343);
#1166=LINE('',#42262,#1344);
#1167=LINE('',#42853,#1345);
#1168=LINE('',#43456,#1346);
#1169=LINE('',#44111,#1347);
#1170=LINE('',#44756,#1348);
#1171=LINE('',#45369,#1349);
#1172=LINE('',#45952,#1350);
#1173=LINE('',#46577,#1351);
#1174=LINE('',#47132,#1352);
#1175=LINE('',#47510,#1353);
#1176=LINE('',#48017,#1354);
#1177=LINE('',#48580,#1355);
#1178=LINE('',#48941,#1356);
#1179=LINE('',#49470,#1357);
#1180=LINE('',#50063,#1358);
#1181=LINE('',#50642,#1359);
#1182=LINE('',#51211,#1360);
#1183=LINE('',#51834,#1361);
#1184=LINE('',#52433,#1362);
#1185=LINE('',#52952,#1363);
#1186=LINE('',#53538,#1364);
#1187=LINE('',#54126,#1365);
#1282=VECTOR('',#5491,3.22275);
#1283=VECTOR('',#5496,3.22275);
#1284=VECTOR('',#5499,3.22275);
#1285=VECTOR('',#5502,3.22275);
#1286=VECTOR('',#5505,3.22275);
#1287=VECTOR('',#5508,3.22275);
#1288=VECTOR('',#5511,3.22275);
#1289=VECTOR('',#5514,3.22275);
#1290=VECTOR('',#5517,3.22275);
#1291=VECTOR('',#5520,3.22275);
#1292=VECTOR('',#5523,3.22275);
#1293=VECTOR('',#5526,3.22275);
#1294=VECTOR('',#5529,3.22275);
#1295=VECTOR('',#5532,3.22275);
#1296=VECTOR('',#5535,3.22275);
#1297=VECTOR('',#5538,3.22275);
#1298=VECTOR('',#5541,3.22275);
#1299=VECTOR('',#5544,3.22275);
#1300=VECTOR('',#5547,3.22275);
#1301=VECTOR('',#5550,3.22275);
#1302=VECTOR('',#5553,3.22275);
#1303=VECTOR('',#5556,3.22275);
#1304=VECTOR('',#5559,3.22275);
#1305=VECTOR('',#5562,3.22275);
#1306=VECTOR('',#5565,3.22275);
#1307=VECTOR('',#5568,3.22275);
#1308=VECTOR('',#5571,3.22275);
#1309=VECTOR('',#5574,3.22275);
#1310=VECTOR('',#5577,3.22275);
#1311=VECTOR('',#5580,3.22275);
#1312=VECTOR('',#5583,3.22275);
#1313=VECTOR('',#5586,3.22275);
#1314=VECTOR('',#5589,3.22275);
#1315=VECTOR('',#5592,3.22275);
#1316=VECTOR('',#5595,3.22275);
#1317=VECTOR('',#5598,3.22275);
#1318=VECTOR('',#5601,3.22275);
#1319=VECTOR('',#5604,3.22275);
#1320=VECTOR('',#5607,3.22275);
#1321=VECTOR('',#5610,3.22275);
#1322=VECTOR('',#5613,3.22275);
#1323=VECTOR('',#5616,3.22275);
#1324=VECTOR('',#5619,3.22275);
#1325=VECTOR('',#5622,3.22275);
#1326=VECTOR('',#5625,3.22275);
#1327=VECTOR('',#5628,3.22275);
#1328=VECTOR('',#5631,3.22275);
#1329=VECTOR('',#5634,3.22275);
#1330=VECTOR('',#5637,3.22275);
#1331=VECTOR('',#5640,3.22275);
#1332=VECTOR('',#5643,3.22275);
#1333=VECTOR('',#5646,3.22275);
#1334=VECTOR('',#5649,3.22275);
#1335=VECTOR('',#5652,3.22275);
#1336=VECTOR('',#5655,3.22275);
#1337=VECTOR('',#5658,3.22275);
#1338=VECTOR('',#5661,3.22275);
#1339=VECTOR('',#5664,3.22275);
#1340=VECTOR('',#5667,3.22275);
#1341=VECTOR('',#5670,3.22275);
#1342=VECTOR('',#5673,3.22275);
#1343=VECTOR('',#5676,3.22275);
#1344=VECTOR('',#5679,3.22275);
#1345=VECTOR('',#5682,3.22275);
#1346=VECTOR('',#5685,3.22275);
#1347=VECTOR('',#5688,3.22275);
#1348=VECTOR('',#5691,3.22275);
#1349=VECTOR('',#5694,3.22275);
#1350=VECTOR('',#5697,3.22275);
#1351=VECTOR('',#5700,3.22275);
#1352=VECTOR('',#5703,3.22275);
#1353=VECTOR('',#5706,3.22275);
#1354=VECTOR('',#5709,3.22275);
#1355=VECTOR('',#5712,3.22275);
#1356=VECTOR('',#5715,3.22275);
#1357=VECTOR('',#5718,3.22275);
#1358=VECTOR('',#5721,3.22275);
#1359=VECTOR('',#5724,3.22275);
#1360=VECTOR('',#5727,3.22275);
#1361=VECTOR('',#5730,3.22275);
#1362=VECTOR('',#5733,3.22275);
#1363=VECTOR('',#5736,3.22275);
#1364=VECTOR('',#5739,3.22275);
#1365=VECTOR('',#5742,3.22275);
#1457=CIRCLE('',#4847,3.22275);
#1458=CIRCLE('',#4932,3.933);
#1459=CIRCLE('',#4933,3.933);
#1460=CIRCLE('',#4935,3.22275);
#1592=VERTEX_POINT('',#6225);
#1593=VERTEX_POINT('',#6226);
#1594=VERTEX_POINT('',#6228);
#1595=VERTEX_POINT('',#6341);
#1596=VERTEX_POINT('',#6414);
#1597=VERTEX_POINT('',#6415);
#1598=VERTEX_POINT('',#6417);
#1599=VERTEX_POINT('',#6709);
#1600=VERTEX_POINT('',#6987);
#1601=VERTEX_POINT('',#6988);
#1602=VERTEX_POINT('',#7565);
#1603=VERTEX_POINT('',#7566);
#1604=VERTEX_POINT('',#7568);
#1605=VERTEX_POINT('',#7879);
#1606=VERTEX_POINT('',#8157);
#1607=VERTEX_POINT('',#8158);
#1608=VERTEX_POINT('',#8709);
#1609=VERTEX_POINT('',#8710);
#1610=VERTEX_POINT('',#8712);
#1611=VERTEX_POINT('',#9017);
#1612=VERTEX_POINT('',#9317);
#1613=VERTEX_POINT('',#9318);
#1614=VERTEX_POINT('',#9899);
#1615=VERTEX_POINT('',#9900);
#1616=VERTEX_POINT('',#9902);
#1617=VERTEX_POINT('',#10209);
#1618=VERTEX_POINT('',#10515);
#1619=VERTEX_POINT('',#10516);
#1620=VERTEX_POINT('',#11061);
#1621=VERTEX_POINT('',#11062);
#1622=VERTEX_POINT('',#11064);
#1623=VERTEX_POINT('',#11371);
#1624=VERTEX_POINT('',#11695);
#1625=VERTEX_POINT('',#11696);
#1626=VERTEX_POINT('',#12259);
#1627=VERTEX_POINT('',#12260);
#1628=VERTEX_POINT('',#12262);
#1629=VERTEX_POINT('',#12565);
#1630=VERTEX_POINT('',#12873);
#1631=VERTEX_POINT('',#12874);
#1632=VERTEX_POINT('',#13437);
#1633=VERTEX_POINT('',#13438);
#1634=VERTEX_POINT('',#13440);
#1635=VERTEX_POINT('',#13761);
#1636=VERTEX_POINT('',#14045);
#1637=VERTEX_POINT('',#14046);
#1638=VERTEX_POINT('',#14613);
#1639=VERTEX_POINT('',#14614);
#1640=VERTEX_POINT('',#14616);
#1641=VERTEX_POINT('',#14955);
#1642=VERTEX_POINT('',#15205);
#1643=VERTEX_POINT('',#15206);
#1644=VERTEX_POINT('',#15494);
#1645=VERTEX_POINT('',#15796);
#1646=VERTEX_POINT('',#15797);
#1647=VERTEX_POINT('',#15799);
#1648=VERTEX_POINT('',#16427);
#1649=VERTEX_POINT('',#16428);
#1650=VERTEX_POINT('',#16724);
#1651=VERTEX_POINT('',#17068);
#1652=VERTEX_POINT('',#17069);
#1653=VERTEX_POINT('',#17071);
#1654=VERTEX_POINT('',#17611);
#1655=VERTEX_POINT('',#17612);
#1656=VERTEX_POINT('',#17908);
#1657=VERTEX_POINT('',#18322);
#1658=VERTEX_POINT('',#18323);
#1659=VERTEX_POINT('',#18325);
#1660=VERTEX_POINT('',#18927);
#1661=VERTEX_POINT('',#18928);
#1662=VERTEX_POINT('',#19270);
#1663=VERTEX_POINT('',#19650);
#1664=VERTEX_POINT('',#19651);
#1665=VERTEX_POINT('',#19653);
#1666=VERTEX_POINT('',#20217);
#1667=VERTEX_POINT('',#20218);
#1668=VERTEX_POINT('',#20504);
#1669=VERTEX_POINT('',#20834);
#1670=VERTEX_POINT('',#20835);
#1671=VERTEX_POINT('',#20837);
#1672=VERTEX_POINT('',#21421);
#1673=VERTEX_POINT('',#21422);
#1674=VERTEX_POINT('',#21736);
#1675=VERTEX_POINT('',#22024);
#1676=VERTEX_POINT('',#22025);
#1677=VERTEX_POINT('',#22027);
#1678=VERTEX_POINT('',#22617);
#1679=VERTEX_POINT('',#22618);
#1680=VERTEX_POINT('',#22910);
#1681=VERTEX_POINT('',#23220);
#1682=VERTEX_POINT('',#23221);
#1683=VERTEX_POINT('',#23223);
#1684=VERTEX_POINT('',#23825);
#1685=VERTEX_POINT('',#23826);
#1686=VERTEX_POINT('',#24104);
#1687=VERTEX_POINT('',#24390);
#1688=VERTEX_POINT('',#24391);
#1689=VERTEX_POINT('',#24393);
#1690=VERTEX_POINT('',#24965);
#1691=VERTEX_POINT('',#24966);
#1692=VERTEX_POINT('',#25236);
#1693=VERTEX_POINT('',#25558);
#1694=VERTEX_POINT('',#25559);
#1695=VERTEX_POINT('',#25561);
#1696=VERTEX_POINT('',#26109);
#1697=VERTEX_POINT('',#26110);
#1698=VERTEX_POINT('',#26412);
#1699=VERTEX_POINT('',#26698);
#1700=VERTEX_POINT('',#26699);
#1701=VERTEX_POINT('',#26701);
#1702=VERTEX_POINT('',#27309);
#1703=VERTEX_POINT('',#27310);
#1704=VERTEX_POINT('',#27640);
#1705=VERTEX_POINT('',#27900);
#1706=VERTEX_POINT('',#27901);
#1707=VERTEX_POINT('',#27903);
#1708=VERTEX_POINT('',#28190);
#1709=VERTEX_POINT('',#28486);
#1710=VERTEX_POINT('',#28487);
#1711=VERTEX_POINT('',#29134);
#1712=VERTEX_POINT('',#29135);
#1713=VERTEX_POINT('',#29137);
#1714=VERTEX_POINT('',#29408);
#1715=VERTEX_POINT('',#29642);
#1716=VERTEX_POINT('',#29643);
#1717=VERTEX_POINT('',#29937);
#1718=VERTEX_POINT('',#30200);
#1719=VERTEX_POINT('',#30201);
#1720=VERTEX_POINT('',#30203);
#1721=VERTEX_POINT('',#30811);
#1722=VERTEX_POINT('',#30812);
#1723=VERTEX_POINT('',#31078);
#1724=VERTEX_POINT('',#31390);
#1725=VERTEX_POINT('',#31391);
#1726=VERTEX_POINT('',#31393);
#1727=VERTEX_POINT('',#31943);
#1728=VERTEX_POINT('',#31944);
#1729=VERTEX_POINT('',#31946);
#1730=VERTEX_POINT('',#32211);
#1731=VERTEX_POINT('',#32461);
#1732=VERTEX_POINT('',#32462);
#1733=VERTEX_POINT('',#32734);
#1734=VERTEX_POINT('',#32988);
#1735=VERTEX_POINT('',#32989);
#1736=VERTEX_POINT('',#32991);
#1737=VERTEX_POINT('',#33613);
#1738=VERTEX_POINT('',#33614);
#1739=VERTEX_POINT('',#33900);
#1740=VERTEX_POINT('',#34194);
#1741=VERTEX_POINT('',#34195);
#1742=VERTEX_POINT('',#34197);
#1743=VERTEX_POINT('',#34861);
#1744=VERTEX_POINT('',#34862);
#1745=VERTEX_POINT('',#35148);
#1746=VERTEX_POINT('',#35394);
#1747=VERTEX_POINT('',#35395);
#1748=VERTEX_POINT('',#35397);
#1749=VERTEX_POINT('',#35634);
#1750=VERTEX_POINT('',#35884);
#1751=VERTEX_POINT('',#35885);
#1752=VERTEX_POINT('',#35887);
#1753=VERTEX_POINT('',#36443);
#1754=VERTEX_POINT('',#36444);
#1755=VERTEX_POINT('',#36766);
#1756=VERTEX_POINT('',#37030);
#1757=VERTEX_POINT('',#37031);
#1758=VERTEX_POINT('',#37033);
#1759=VERTEX_POINT('',#37328);
#1760=VERTEX_POINT('',#37620);
#1761=VERTEX_POINT('',#37621);
#1762=VERTEX_POINT('',#38170);
#1763=VERTEX_POINT('',#38171);
#1764=VERTEX_POINT('',#38173);
#1765=VERTEX_POINT('',#38468);
#1766=VERTEX_POINT('',#38698);
#1767=VERTEX_POINT('',#38699);
#1768=VERTEX_POINT('',#38959);
#1769=VERTEX_POINT('',#39227);
#1770=VERTEX_POINT('',#39228);
#1771=VERTEX_POINT('',#39230);
#1772=VERTEX_POINT('',#39814);
#1773=VERTEX_POINT('',#39815);
#1774=VERTEX_POINT('',#40079);
#1775=VERTEX_POINT('',#40423);
#1776=VERTEX_POINT('',#40424);
#1777=VERTEX_POINT('',#40426);
#1778=VERTEX_POINT('',#41060);
#1779=VERTEX_POINT('',#41061);
#1780=VERTEX_POINT('',#41315);
#1781=VERTEX_POINT('',#41667);
#1782=VERTEX_POINT('',#41668);
#1783=VERTEX_POINT('',#41670);
#1784=VERTEX_POINT('',#42260);
#1785=VERTEX_POINT('',#42261);
#1786=VERTEX_POINT('',#42575);
#1787=VERTEX_POINT('',#42851);
#1788=VERTEX_POINT('',#42852);
#1789=VERTEX_POINT('',#42854);
#1790=VERTEX_POINT('',#43454);
#1791=VERTEX_POINT('',#43455);
#1792=VERTEX_POINT('',#43779);
#1793=VERTEX_POINT('',#44109);
#1794=VERTEX_POINT('',#44110);
#1795=VERTEX_POINT('',#44112);
#1796=VERTEX_POINT('',#44754);
#1797=VERTEX_POINT('',#44755);
#1798=VERTEX_POINT('',#45055);
#1799=VERTEX_POINT('',#45367);
#1800=VERTEX_POINT('',#45368);
#1801=VERTEX_POINT('',#45370);
#1802=VERTEX_POINT('',#45950);
#1803=VERTEX_POINT('',#45951);
#1804=VERTEX_POINT('',#46251);
#1805=VERTEX_POINT('',#46575);
#1806=VERTEX_POINT('',#46576);
#1807=VERTEX_POINT('',#46578);
#1808=VERTEX_POINT('',#47130);
#1809=VERTEX_POINT('',#47131);
#1810=VERTEX_POINT('',#47133);
#1811=VERTEX_POINT('',#47212);
#1812=VERTEX_POINT('',#47508);
#1813=VERTEX_POINT('',#47509);
#1814=VERTEX_POINT('',#47511);
#1815=VERTEX_POINT('',#48015);
#1816=VERTEX_POINT('',#48016);
#1817=VERTEX_POINT('',#48340);
#1818=VERTEX_POINT('',#48578);
#1819=VERTEX_POINT('',#48579);
#1820=VERTEX_POINT('',#48581);
#1821=VERTEX_POINT('',#48681);
#1822=VERTEX_POINT('',#48939);
#1823=VERTEX_POINT('',#48940);
#1824=VERTEX_POINT('',#48942);
#1825=VERTEX_POINT('',#49468);
#1826=VERTEX_POINT('',#49469);
#1827=VERTEX_POINT('',#49761);
#1828=VERTEX_POINT('',#50061);
#1829=VERTEX_POINT('',#50062);
#1830=VERTEX_POINT('',#50064);
#1831=VERTEX_POINT('',#50640);
#1832=VERTEX_POINT('',#50641);
#1833=VERTEX_POINT('',#50915);
#1834=VERTEX_POINT('',#51209);
#1835=VERTEX_POINT('',#51210);
#1836=VERTEX_POINT('',#51212);
#1837=VERTEX_POINT('',#51832);
#1838=VERTEX_POINT('',#51833);
#1839=VERTEX_POINT('',#52121);
#1840=VERTEX_POINT('',#52431);
#1841=VERTEX_POINT('',#52432);
#1842=VERTEX_POINT('',#52434);
#1843=VERTEX_POINT('',#52950);
#1844=VERTEX_POINT('',#52951);
#1845=VERTEX_POINT('',#52953);
#1846=VERTEX_POINT('',#53206);
#1847=VERTEX_POINT('',#53536);
#1848=VERTEX_POINT('',#53537);
#1849=VERTEX_POINT('',#54124);
#1850=VERTEX_POINT('',#54125);
#1851=VERTEX_POINT('',#54127);
#1852=VERTEX_POINT('',#54360);
#1853=VERTEX_POINT('',#54676);
#1854=VERTEX_POINT('',#54677);
#1855=VERTEX_POINT('',#54751);
#1856=VERTEX_POINT('',#54753);
#1857=VERTEX_POINT('',#54759);
#1858=VERTEX_POINT('',#54986);
#1859=VERTEX_POINT('',#54997);
#1860=VERTEX_POINT('',#55008);
#1861=VERTEX_POINT('',#55238);
#1862=VERTEX_POINT('',#55249);
#1863=VERTEX_POINT('',#55476);
#1864=VERTEX_POINT('',#55488);
#1865=VERTEX_POINT('',#55499);
#1866=VERTEX_POINT('',#55510);
#1867=VERTEX_POINT('',#55521);
#1868=VERTEX_POINT('',#55751);
#1869=VERTEX_POINT('',#55762);
#1870=VERTEX_POINT('',#55773);
#1871=VERTEX_POINT('',#56000);
#1872=VERTEX_POINT('',#56011);
#1873=VERTEX_POINT('',#56238);
#1874=VERTEX_POINT('',#56249);
#1875=VERTEX_POINT('',#56262);
#1876=VERTEX_POINT('',#56273);
#1877=VERTEX_POINT('',#56284);
#1878=VERTEX_POINT('',#56511);
#1879=VERTEX_POINT('',#56522);
#1880=VERTEX_POINT('',#56749);
#1881=VERTEX_POINT('',#56760);
#1882=VERTEX_POINT('',#56773);
#1883=VERTEX_POINT('',#56784);
#1884=VERTEX_POINT('',#56795);
#1885=VERTEX_POINT('',#57022);
#1886=VERTEX_POINT('',#57033);
#1887=VERTEX_POINT('',#57260);
#1888=VERTEX_POINT('',#57271);
#1889=VERTEX_POINT('',#57283);
#1890=VERTEX_POINT('',#57294);
#1891=VERTEX_POINT('',#57305);
#1892=VERTEX_POINT('',#57317);
#1893=VERTEX_POINT('',#57328);
#1894=VERTEX_POINT('',#57339);
#1895=VERTEX_POINT('',#57566);
#1896=VERTEX_POINT('',#57579);
#1897=VERTEX_POINT('',#57806);
#1898=VERTEX_POINT('',#58033);
#1899=VERTEX_POINT('',#58045);
#1900=VERTEX_POINT('',#58056);
#1901=VERTEX_POINT('',#58067);
#1902=VERTEX_POINT('',#58294);
#1903=VERTEX_POINT('',#58307);
#1904=VERTEX_POINT('',#58534);
#1905=VERTEX_POINT('',#58761);
#1906=VERTEX_POINT('',#58773);
#1907=VERTEX_POINT('',#58784);
#1908=VERTEX_POINT('',#58795);
#1909=VERTEX_POINT('',#59022);
#1910=VERTEX_POINT('',#59034);
#1911=VERTEX_POINT('',#59045);
#1912=VERTEX_POINT('',#59056);
#1913=VERTEX_POINT('',#59068);
#1914=VERTEX_POINT('',#59295);
#1915=VERTEX_POINT('',#59306);
#1916=VERTEX_POINT('',#59317);
#1917=VERTEX_POINT('',#59329);
#1918=VERTEX_POINT('',#59556);
#1919=VERTEX_POINT('',#59783);
#1920=VERTEX_POINT('',#59795);
#1921=VERTEX_POINT('',#60022);
#1922=VERTEX_POINT('',#60033);
#1923=VERTEX_POINT('',#60044);
#1924=VERTEX_POINT('',#60056);
#1925=VERTEX_POINT('',#60283);
#1926=VERTEX_POINT('',#60510);
#1927=VERTEX_POINT('',#60522);
#1928=VERTEX_POINT('',#60749);
#1929=VERTEX_POINT('',#60760);
#1930=VERTEX_POINT('',#60771);
#1931=VERTEX_POINT('',#60998);
#1932=VERTEX_POINT('',#61009);
#1933=VERTEX_POINT('',#61020);
#1934=VERTEX_POINT('',#61032);
#1935=VERTEX_POINT('',#61043);
#1936=VERTEX_POINT('',#61270);
#1937=VERTEX_POINT('',#61281);
#1938=VERTEX_POINT('',#61508);
#1939=VERTEX_POINT('',#61519);
#1940=VERTEX_POINT('',#61530);
#1941=VERTEX_POINT('',#61715);
#1942=VERTEX_POINT('',#61717);
#1943=VERTEX_POINT('',#61726);
#1944=VERTEX_POINT('',#61737);
#1945=VERTEX_POINT('',#61964);
#1946=VERTEX_POINT('',#61976);
#1947=VERTEX_POINT('',#61987);
#1948=VERTEX_POINT('',#61998);
#1949=VERTEX_POINT('',#62009);
#1950=VERTEX_POINT('',#62239);
#1951=VERTEX_POINT('',#62250);
#1952=VERTEX_POINT('',#62261);
#1953=VERTEX_POINT('',#62273);
#1954=VERTEX_POINT('',#62284);
#1955=VERTEX_POINT('',#62511);
#1956=VERTEX_POINT('',#62522);
#1957=VERTEX_POINT('',#62752);
#1958=VERTEX_POINT('',#62763);
#1959=VERTEX_POINT('',#62774);
#1960=VERTEX_POINT('',#63001);
#1961=VERTEX_POINT('',#63012);
#1962=VERTEX_POINT('',#63239);
#1963=VERTEX_POINT('',#63250);
#1964=VERTEX_POINT('',#63263);
#1965=VERTEX_POINT('',#63274);
#1966=VERTEX_POINT('',#63285);
#1967=VERTEX_POINT('',#63512);
#1968=VERTEX_POINT('',#63523);
#1969=VERTEX_POINT('',#63750);
#1970=VERTEX_POINT('',#63761);
#1971=VERTEX_POINT('',#63774);
#1972=VERTEX_POINT('',#63785);
#1973=VERTEX_POINT('',#63796);
#1974=VERTEX_POINT('',#64023);
#1975=VERTEX_POINT('',#64034);
#1976=VERTEX_POINT('',#64261);
#1977=VERTEX_POINT('',#64488);
#1978=VERTEX_POINT('',#64501);
#1979=VERTEX_POINT('',#64728);
#1980=VERTEX_POINT('',#64955);
#1981=VERTEX_POINT('',#64967);
#1982=VERTEX_POINT('',#64978);
#1983=VERTEX_POINT('',#64989);
#1984=VERTEX_POINT('',#65216);
#1985=VERTEX_POINT('',#65229);
#1986=VERTEX_POINT('',#65456);
#1987=VERTEX_POINT('',#65683);
#1988=VERTEX_POINT('',#65695);
#1989=VERTEX_POINT('',#65706);
#1990=VERTEX_POINT('',#65717);
#1991=VERTEX_POINT('',#65944);
#1992=VERTEX_POINT('',#65957);
#1993=VERTEX_POINT('',#65968);
#1994=VERTEX_POINT('',#65979);
#1995=VERTEX_POINT('',#65991);
#1996=VERTEX_POINT('',#66218);
#1997=VERTEX_POINT('',#66229);
#1998=VERTEX_POINT('',#66456);
#1999=VERTEX_POINT('',#66468);
#2000=VERTEX_POINT('',#66695);
#2001=VERTEX_POINT('',#66922);
#2002=VERTEX_POINT('',#66934);
#2003=VERTEX_POINT('',#67161);
#2004=VERTEX_POINT('',#67172);
#2005=VERTEX_POINT('',#67183);
#2006=VERTEX_POINT('',#67196);
#2007=VERTEX_POINT('',#67423);
#2008=VERTEX_POINT('',#67650);
#2009=VERTEX_POINT('',#67662);
#2010=VERTEX_POINT('',#67889);
#2011=VERTEX_POINT('',#67900);
#2012=VERTEX_POINT('',#67911);
#2013=VERTEX_POINT('',#67923);
#2014=VERTEX_POINT('',#68153);
#2015=VERTEX_POINT('',#68380);
#2016=VERTEX_POINT('',#68392);
#2017=VERTEX_POINT('',#68403);
#2018=VERTEX_POINT('',#68630);
#2019=VERTEX_POINT('',#68641);
#2020=VERTEX_POINT('',#68868);
#2021=VERTEX_POINT('',#68879);
#2022=VERTEX_POINT('',#68890);
#2023=VERTEX_POINT('',#68902);
#2024=VERTEX_POINT('',#68913);
#2025=VERTEX_POINT('',#69151);
#2026=VERTEX_POINT('',#69326);
#2027=VERTEX_POINT('',#69328);
#2028=VERTEX_POINT('',#73885);
#2246=EDGE_CURVE('',#1592,#1593,#1104,.T.);
#2247=EDGE_CURVE('',#1594,#1592,#49,.T.);
#2248=EDGE_CURVE('',#1595,#1594,#1457,.T.);
#2249=EDGE_CURVE('',#1595,#1593,#50,.T.);
#2250=EDGE_CURVE('',#1596,#1597,#1105,.T.);
#2251=EDGE_CURVE('',#1598,#1596,#51,.F.);
#2252=EDGE_CURVE('',#1592,#1598,#52,.T.);
#2253=EDGE_CURVE('',#1593,#1599,#53,.T.);
#2254=EDGE_CURVE('',#1599,#1597,#54,.T.);
#2255=EDGE_CURVE('',#1600,#1601,#1106,.T.);
#2256=EDGE_CURVE('',#1596,#1600,#55,.F.);
#2257=EDGE_CURVE('',#1597,#1601,#56,.T.);
#2258=EDGE_CURVE('',#1602,#1603,#1107,.T.);
#2259=EDGE_CURVE('',#1604,#1602,#57,.F.);
#2260=EDGE_CURVE('',#1600,#1604,#58,.F.);
#2261=EDGE_CURVE('',#1601,#1605,#59,.T.);
#2262=EDGE_CURVE('',#1605,#1603,#60,.T.);
#2263=EDGE_CURVE('',#1606,#1607,#1108,.T.);
#2264=EDGE_CURVE('',#1602,#1606,#61,.F.);
#2265=EDGE_CURVE('',#1603,#1607,#62,.T.);
#2266=EDGE_CURVE('',#1608,#1609,#1109,.T.);
#2267=EDGE_CURVE('',#1610,#1608,#63,.F.);
#2268=EDGE_CURVE('',#1606,#1610,#64,.F.);
#2269=EDGE_CURVE('',#1607,#1611,#65,.T.);
#2270=EDGE_CURVE('',#1611,#1609,#66,.T.);
#2271=EDGE_CURVE('',#1612,#1613,#1110,.T.);
#2272=EDGE_CURVE('',#1608,#1612,#67,.F.);
#2273=EDGE_CURVE('',#1609,#1613,#68,.T.);
#2274=EDGE_CURVE('',#1614,#1615,#1111,.T.);
#2275=EDGE_CURVE('',#1616,#1614,#69,.F.);
#2276=EDGE_CURVE('',#1612,#1616,#70,.F.);
#2277=EDGE_CURVE('',#1613,#1617,#71,.T.);
#2278=EDGE_CURVE('',#1617,#1615,#72,.T.);
#2279=EDGE_CURVE('',#1618,#1619,#1112,.T.);
#2280=EDGE_CURVE('',#1614,#1618,#73,.F.);
#2281=EDGE_CURVE('',#1615,#1619,#74,.T.);
#2282=EDGE_CURVE('',#1620,#1621,#1113,.T.);
#2283=EDGE_CURVE('',#1622,#1620,#75,.F.);
#2284=EDGE_CURVE('',#1618,#1622,#76,.F.);
#2285=EDGE_CURVE('',#1619,#1623,#77,.T.);
#2286=EDGE_CURVE('',#1623,#1621,#78,.T.);
#2287=EDGE_CURVE('',#1624,#1625,#1114,.T.);
#2288=EDGE_CURVE('',#1620,#1624,#79,.F.);
#2289=EDGE_CURVE('',#1621,#1625,#80,.T.);
#2290=EDGE_CURVE('',#1626,#1627,#1115,.T.);
#2291=EDGE_CURVE('',#1628,#1626,#81,.F.);
#2292=EDGE_CURVE('',#1624,#1628,#82,.F.);
#2293=EDGE_CURVE('',#1625,#1629,#83,.T.);
#2294=EDGE_CURVE('',#1629,#1627,#84,.T.);
#2295=EDGE_CURVE('',#1630,#1631,#1116,.T.);
#2296=EDGE_CURVE('',#1626,#1630,#85,.F.);
#2297=EDGE_CURVE('',#1627,#1631,#86,.T.);
#2298=EDGE_CURVE('',#1632,#1633,#1117,.T.);
#2299=EDGE_CURVE('',#1634,#1632,#87,.F.);
#2300=EDGE_CURVE('',#1630,#1634,#88,.F.);
#2301=EDGE_CURVE('',#1631,#1635,#89,.T.);
#2302=EDGE_CURVE('',#1635,#1633,#90,.T.);
#2303=EDGE_CURVE('',#1636,#1637,#1118,.T.);
#2304=EDGE_CURVE('',#1632,#1636,#91,.F.);
#2305=EDGE_CURVE('',#1633,#1637,#92,.T.);
#2306=EDGE_CURVE('',#1638,#1639,#1119,.T.);
#2307=EDGE_CURVE('',#1640,#1638,#93,.F.);
#2308=EDGE_CURVE('',#1636,#1640,#94,.F.);
#2309=EDGE_CURVE('',#1637,#1641,#95,.T.);
#2310=EDGE_CURVE('',#1641,#1639,#96,.T.);
#2311=EDGE_CURVE('',#1642,#1643,#1120,.T.);
#2312=EDGE_CURVE('',#1638,#1642,#97,.F.);
#2313=EDGE_CURVE('',#1639,#1644,#98,.T.);
#2314=EDGE_CURVE('',#1644,#1643,#99,.T.);
#2315=EDGE_CURVE('',#1645,#1646,#1121,.T.);
#2316=EDGE_CURVE('',#1647,#1645,#100,.F.);
#2317=EDGE_CURVE('',#1642,#1647,#101,.F.);
#2318=EDGE_CURVE('',#1643,#1646,#102,.T.);
#2319=EDGE_CURVE('',#1648,#1649,#1122,.T.);
#2320=EDGE_CURVE('',#1645,#1648,#103,.F.);
#2321=EDGE_CURVE('',#1646,#1650,#104,.T.);
#2322=EDGE_CURVE('',#1650,#1649,#105,.T.);
#2323=EDGE_CURVE('',#1651,#1652,#1123,.T.);
#2324=EDGE_CURVE('',#1653,#1651,#106,.F.);
#2325=EDGE_CURVE('',#1648,#1653,#107,.F.);
#2326=EDGE_CURVE('',#1649,#1652,#108,.T.);
#2327=EDGE_CURVE('',#1654,#1655,#1124,.T.);
#2328=EDGE_CURVE('',#1651,#1654,#109,.F.);
#2329=EDGE_CURVE('',#1652,#1656,#110,.T.);
#2330=EDGE_CURVE('',#1656,#1655,#111,.T.);
#2331=EDGE_CURVE('',#1657,#1658,#1125,.T.);
#2332=EDGE_CURVE('',#1659,#1657,#112,.F.);
#2333=EDGE_CURVE('',#1654,#1659,#113,.F.);
#2334=EDGE_CURVE('',#1655,#1658,#114,.T.);
#2335=EDGE_CURVE('',#1660,#1661,#1126,.T.);
#2336=EDGE_CURVE('',#1657,#1660,#115,.F.);
#2337=EDGE_CURVE('',#1658,#1662,#116,.T.);
#2338=EDGE_CURVE('',#1662,#1661,#117,.T.);
#2339=EDGE_CURVE('',#1663,#1664,#1127,.T.);
#2340=EDGE_CURVE('',#1665,#1663,#118,.F.);
#2341=EDGE_CURVE('',#1660,#1665,#119,.F.);
#2342=EDGE_CURVE('',#1661,#1664,#120,.T.);
#2343=EDGE_CURVE('',#1666,#1667,#1128,.T.);
#2344=EDGE_CURVE('',#1663,#1666,#121,.F.);
#2345=EDGE_CURVE('',#1664,#1668,#122,.T.);
#2346=EDGE_CURVE('',#1668,#1667,#123,.T.);
#2347=EDGE_CURVE('',#1669,#1670,#1129,.T.);
#2348=EDGE_CURVE('',#1671,#1669,#124,.F.);
#2349=EDGE_CURVE('',#1666,#1671,#125,.F.);
#2350=EDGE_CURVE('',#1667,#1670,#126,.T.);
#2351=EDGE_CURVE('',#1672,#1673,#1130,.T.);
#2352=EDGE_CURVE('',#1669,#1672,#127,.F.);
#2353=EDGE_CURVE('',#1670,#1674,#128,.T.);
#2354=EDGE_CURVE('',#1674,#1673,#129,.T.);
#2355=EDGE_CURVE('',#1675,#1676,#1131,.T.);
#2356=EDGE_CURVE('',#1677,#1675,#130,.F.);
#2357=EDGE_CURVE('',#1672,#1677,#131,.F.);
#2358=EDGE_CURVE('',#1673,#1676,#132,.T.);
#2359=EDGE_CURVE('',#1678,#1679,#1132,.T.);
#2360=EDGE_CURVE('',#1675,#1678,#133,.F.);
#2361=EDGE_CURVE('',#1676,#1680,#134,.T.);
#2362=EDGE_CURVE('',#1680,#1679,#135,.T.);
#2363=EDGE_CURVE('',#1681,#1682,#1133,.T.);
#2364=EDGE_CURVE('',#1683,#1681,#136,.F.);
#2365=EDGE_CURVE('',#1678,#1683,#137,.F.);
#2366=EDGE_CURVE('',#1679,#1682,#138,.T.);
#2367=EDGE_CURVE('',#1684,#1685,#1134,.T.);
#2368=EDGE_CURVE('',#1681,#1684,#139,.F.);
#2369=EDGE_CURVE('',#1682,#1686,#140,.T.);
#2370=EDGE_CURVE('',#1686,#1685,#141,.T.);
#2371=EDGE_CURVE('',#1687,#1688,#1135,.T.);
#2372=EDGE_CURVE('',#1689,#1687,#142,.F.);
#2373=EDGE_CURVE('',#1684,#1689,#143,.F.);
#2374=EDGE_CURVE('',#1685,#1688,#144,.T.);
#2375=EDGE_CURVE('',#1690,#1691,#1136,.T.);
#2376=EDGE_CURVE('',#1687,#1690,#145,.F.);
#2377=EDGE_CURVE('',#1688,#1692,#146,.T.);
#2378=EDGE_CURVE('',#1692,#1691,#147,.T.);
#2379=EDGE_CURVE('',#1693,#1694,#1137,.T.);
#2380=EDGE_CURVE('',#1695,#1693,#148,.F.);
#2381=EDGE_CURVE('',#1690,#1695,#149,.F.);
#2382=EDGE_CURVE('',#1691,#1694,#150,.T.);
#2383=EDGE_CURVE('',#1696,#1697,#1138,.T.);
#2384=EDGE_CURVE('',#1693,#1696,#151,.F.);
#2385=EDGE_CURVE('',#1694,#1698,#152,.T.);
#2386=EDGE_CURVE('',#1698,#1697,#153,.T.);
#2387=EDGE_CURVE('',#1699,#1700,#1139,.T.);
#2388=EDGE_CURVE('',#1701,#1699,#154,.F.);
#2389=EDGE_CURVE('',#1696,#1701,#155,.F.);
#2390=EDGE_CURVE('',#1697,#1700,#156,.T.);
#2391=EDGE_CURVE('',#1702,#1703,#1140,.T.);
#2392=EDGE_CURVE('',#1699,#1702,#157,.F.);
#2393=EDGE_CURVE('',#1700,#1704,#158,.T.);
#2394=EDGE_CURVE('',#1704,#1703,#159,.T.);
#2395=EDGE_CURVE('',#1705,#1706,#1141,.T.);
#2396=EDGE_CURVE('',#1707,#1705,#160,.F.);
#2397=EDGE_CURVE('',#1702,#1707,#161,.F.);
#2398=EDGE_CURVE('',#1703,#1708,#162,.T.);
#2399=EDGE_CURVE('',#1708,#1706,#163,.T.);
#2400=EDGE_CURVE('',#1709,#1710,#1142,.T.);
#2401=EDGE_CURVE('',#1705,#1709,#164,.F.);
#2402=EDGE_CURVE('',#1706,#1710,#165,.T.);
#2403=EDGE_CURVE('',#1711,#1712,#1143,.T.);
#2404=EDGE_CURVE('',#1713,#1711,#166,.F.);
#2405=EDGE_CURVE('',#1709,#1713,#167,.F.);
#2406=EDGE_CURVE('',#1710,#1714,#168,.T.);
#2407=EDGE_CURVE('',#1714,#1712,#169,.T.);
#2408=EDGE_CURVE('',#1715,#1716,#1144,.T.);
#2409=EDGE_CURVE('',#1711,#1715,#170,.F.);
#2410=EDGE_CURVE('',#1712,#1717,#171,.T.);
#2411=EDGE_CURVE('',#1717,#1716,#172,.T.);
#2412=EDGE_CURVE('',#1718,#1719,#1145,.T.);
#2413=EDGE_CURVE('',#1720,#1718,#173,.F.);
#2414=EDGE_CURVE('',#1715,#1720,#174,.F.);
#2415=EDGE_CURVE('',#1716,#1719,#175,.T.);
#2416=EDGE_CURVE('',#1721,#1722,#1146,.T.);
#2417=EDGE_CURVE('',#1718,#1721,#176,.F.);
#2418=EDGE_CURVE('',#1719,#1723,#177,.T.);
#2419=EDGE_CURVE('',#1723,#1722,#178,.T.);
#2420=EDGE_CURVE('',#1724,#1725,#1147,.T.);
#2421=EDGE_CURVE('',#1726,#1724,#179,.T.);
#2422=EDGE_CURVE('',#1721,#1726,#180,.F.);
#2423=EDGE_CURVE('',#1722,#1725,#181,.T.);
#2424=EDGE_CURVE('',#1727,#1728,#1148,.T.);
#2425=EDGE_CURVE('',#1729,#1727,#182,.F.);
#2426=EDGE_CURVE('',#1724,#1729,#183,.T.);
#2427=EDGE_CURVE('',#1725,#1730,#184,.T.);
#2428=EDGE_CURVE('',#1730,#1728,#185,.T.);
#2429=EDGE_CURVE('',#1731,#1732,#1149,.T.);
#2430=EDGE_CURVE('',#1727,#1731,#186,.F.);
#2431=EDGE_CURVE('',#1728,#1733,#187,.T.);
#2432=EDGE_CURVE('',#1733,#1732,#188,.T.);
#2433=EDGE_CURVE('',#1734,#1735,#1150,.T.);
#2434=EDGE_CURVE('',#1736,#1734,#189,.F.);
#2435=EDGE_CURVE('',#1731,#1736,#190,.F.);
#2436=EDGE_CURVE('',#1732,#1735,#191,.T.);
#2437=EDGE_CURVE('',#1737,#1738,#1151,.T.);
#2438=EDGE_CURVE('',#1734,#1737,#192,.F.);
#2439=EDGE_CURVE('',#1735,#1739,#193,.T.);
#2440=EDGE_CURVE('',#1739,#1738,#194,.T.);
#2441=EDGE_CURVE('',#1740,#1741,#1152,.T.);
#2442=EDGE_CURVE('',#1742,#1740,#195,.F.);
#2443=EDGE_CURVE('',#1737,#1742,#196,.F.);
#2444=EDGE_CURVE('',#1738,#1741,#197,.T.);
#2445=EDGE_CURVE('',#1743,#1744,#1153,.T.);
#2446=EDGE_CURVE('',#1740,#1743,#198,.F.);
#2447=EDGE_CURVE('',#1741,#1745,#199,.T.);
#2448=EDGE_CURVE('',#1745,#1744,#200,.T.);
#2449=EDGE_CURVE('',#1746,#1747,#1154,.T.);
#2450=EDGE_CURVE('',#1748,#1746,#201,.T.);
#2451=EDGE_CURVE('',#1743,#1748,#202,.F.);
#2452=EDGE_CURVE('',#1744,#1749,#203,.T.);
#2453=EDGE_CURVE('',#1749,#1747,#204,.T.);
#2454=EDGE_CURVE('',#1750,#1751,#1155,.T.);
#2455=EDGE_CURVE('',#1752,#1750,#205,.F.);
#2456=EDGE_CURVE('',#1746,#1752,#206,.T.);
#2457=EDGE_CURVE('',#1747,#1751,#207,.T.);
#2458=EDGE_CURVE('',#1753,#1754,#1156,.T.);
#2459=EDGE_CURVE('',#1750,#1753,#208,.F.);
#2460=EDGE_CURVE('',#1751,#1755,#209,.T.);
#2461=EDGE_CURVE('',#1755,#1754,#210,.T.);
#2462=EDGE_CURVE('',#1756,#1757,#1157,.T.);
#2463=EDGE_CURVE('',#1758,#1756,#211,.F.);
#2464=EDGE_CURVE('',#1753,#1758,#212,.F.);
#2465=EDGE_CURVE('',#1754,#1759,#213,.T.);
#2466=EDGE_CURVE('',#1759,#1757,#214,.T.);
#2467=EDGE_CURVE('',#1760,#1761,#1158,.T.);
#2468=EDGE_CURVE('',#1756,#1760,#215,.F.);
#2469=EDGE_CURVE('',#1757,#1761,#216,.T.);
#2470=EDGE_CURVE('',#1762,#1763,#1159,.T.);
#2471=EDGE_CURVE('',#1764,#1762,#217,.F.);
#2472=EDGE_CURVE('',#1760,#1764,#218,.F.);
#2473=EDGE_CURVE('',#1761,#1765,#219,.T.);
#2474=EDGE_CURVE('',#1765,#1763,#220,.T.);
#2475=EDGE_CURVE('',#1766,#1767,#1160,.T.);
#2476=EDGE_CURVE('',#1762,#1766,#221,.F.);
#2477=EDGE_CURVE('',#1763,#1768,#222,.T.);
#2478=EDGE_CURVE('',#1768,#1767,#223,.T.);
#2479=EDGE_CURVE('',#1769,#1770,#1161,.T.);
#2480=EDGE_CURVE('',#1771,#1769,#224,.F.);
#2481=EDGE_CURVE('',#1766,#1771,#225,.F.);
#2482=EDGE_CURVE('',#1767,#1770,#226,.T.);
#2483=EDGE_CURVE('',#1772,#1773,#1162,.T.);
#2484=EDGE_CURVE('',#1769,#1772,#227,.F.);
#2485=EDGE_CURVE('',#1770,#1774,#228,.T.);
#2486=EDGE_CURVE('',#1774,#1773,#229,.T.);
#2487=EDGE_CURVE('',#1775,#1776,#1163,.T.);
#2488=EDGE_CURVE('',#1777,#1775,#230,.F.);
#2489=EDGE_CURVE('',#1772,#1777,#231,.F.);
#2490=EDGE_CURVE('',#1773,#1776,#232,.T.);
#2491=EDGE_CURVE('',#1778,#1779,#1164,.T.);
#2492=EDGE_CURVE('',#1775,#1778,#233,.F.);
#2493=EDGE_CURVE('',#1776,#1780,#234,.T.);
#2494=EDGE_CURVE('',#1780,#1779,#235,.T.);
#2495=EDGE_CURVE('',#1781,#1782,#1165,.T.);
#2496=EDGE_CURVE('',#1783,#1781,#236,.F.);
#2497=EDGE_CURVE('',#1778,#1783,#237,.F.);
#2498=EDGE_CURVE('',#1779,#1782,#238,.T.);
#2499=EDGE_CURVE('',#1784,#1785,#1166,.T.);
#2500=EDGE_CURVE('',#1781,#1784,#239,.F.);
#2501=EDGE_CURVE('',#1782,#1786,#240,.T.);
#2502=EDGE_CURVE('',#1786,#1785,#241,.T.);
#2503=EDGE_CURVE('',#1787,#1788,#1167,.T.);
#2504=EDGE_CURVE('',#1789,#1787,#242,.F.);
#2505=EDGE_CURVE('',#1784,#1789,#243,.F.);
#2506=EDGE_CURVE('',#1785,#1788,#244,.T.);
#2507=EDGE_CURVE('',#1790,#1791,#1168,.T.);
#2508=EDGE_CURVE('',#1787,#1790,#245,.F.);
#2509=EDGE_CURVE('',#1788,#1792,#246,.T.);
#2510=EDGE_CURVE('',#1792,#1791,#247,.T.);
#2511=EDGE_CURVE('',#1793,#1794,#1169,.T.);
#2512=EDGE_CURVE('',#1795,#1793,#248,.F.);
#2513=EDGE_CURVE('',#1790,#1795,#249,.F.);
#2514=EDGE_CURVE('',#1791,#1794,#250,.T.);
#2515=EDGE_CURVE('',#1796,#1797,#1170,.T.);
#2516=EDGE_CURVE('',#1793,#1796,#251,.F.);
#2517=EDGE_CURVE('',#1794,#1798,#252,.T.);
#2518=EDGE_CURVE('',#1798,#1797,#253,.T.);
#2519=EDGE_CURVE('',#1799,#1800,#1171,.T.);
#2520=EDGE_CURVE('',#1801,#1799,#254,.F.);
#2521=EDGE_CURVE('',#1796,#1801,#255,.F.);
#2522=EDGE_CURVE('',#1797,#1800,#256,.T.);
#2523=EDGE_CURVE('',#1802,#1803,#1172,.T.);
#2524=EDGE_CURVE('',#1799,#1802,#257,.F.);
#2525=EDGE_CURVE('',#1800,#1804,#258,.T.);
#2526=EDGE_CURVE('',#1804,#1803,#259,.T.);
#2527=EDGE_CURVE('',#1805,#1806,#1173,.T.);
#2528=EDGE_CURVE('',#1807,#1805,#260,.T.);
#2529=EDGE_CURVE('',#1802,#1807,#261,.F.);
#2530=EDGE_CURVE('',#1803,#1806,#262,.T.);
#2531=EDGE_CURVE('',#1808,#1809,#1174,.T.);
#2532=EDGE_CURVE('',#1810,#1808,#263,.T.);
#2533=EDGE_CURVE('',#1805,#1810,#264,.T.);
#2534=EDGE_CURVE('',#1806,#1811,#265,.T.);
#2535=EDGE_CURVE('',#1811,#1809,#266,.T.);
#2536=EDGE_CURVE('',#1812,#1813,#1175,.T.);
#2537=EDGE_CURVE('',#1814,#1812,#267,.F.);
#2538=EDGE_CURVE('',#1808,#1814,#268,.T.);
#2539=EDGE_CURVE('',#1809,#1813,#269,.T.);
#2540=EDGE_CURVE('',#1815,#1816,#1176,.T.);
#2541=EDGE_CURVE('',#1812,#1815,#270,.F.);
#2542=EDGE_CURVE('',#1813,#1817,#271,.T.);
#2543=EDGE_CURVE('',#1817,#1816,#272,.T.);
#2544=EDGE_CURVE('',#1818,#1819,#1177,.T.);
#2545=EDGE_CURVE('',#1820,#1818,#273,.T.);
#2546=EDGE_CURVE('',#1815,#1820,#274,.F.);
#2547=EDGE_CURVE('',#1816,#1821,#275,.T.);
#2548=EDGE_CURVE('',#1821,#1819,#276,.T.);
#2549=EDGE_CURVE('',#1822,#1823,#1178,.T.);
#2550=EDGE_CURVE('',#1824,#1822,#277,.F.);
#2551=EDGE_CURVE('',#1818,#1824,#278,.T.);
#2552=EDGE_CURVE('',#1819,#1823,#279,.T.);
#2553=EDGE_CURVE('',#1825,#1826,#1179,.T.);
#2554=EDGE_CURVE('',#1822,#1825,#280,.F.);
#2555=EDGE_CURVE('',#1823,#1827,#281,.T.);
#2556=EDGE_CURVE('',#1827,#1826,#282,.T.);
#2557=EDGE_CURVE('',#1828,#1829,#1180,.T.);
#2558=EDGE_CURVE('',#1830,#1828,#283,.F.);
#2559=EDGE_CURVE('',#1825,#1830,#284,.F.);
#2560=EDGE_CURVE('',#1826,#1829,#285,.T.);
#2561=EDGE_CURVE('',#1831,#1832,#1181,.T.);
#2562=EDGE_CURVE('',#1828,#1831,#286,.F.);
#2563=EDGE_CURVE('',#1829,#1833,#287,.T.);
#2564=EDGE_CURVE('',#1833,#1832,#288,.T.);
#2565=EDGE_CURVE('',#1834,#1835,#1182,.T.);
#2566=EDGE_CURVE('',#1836,#1834,#289,.F.);
#2567=EDGE_CURVE('',#1831,#1836,#290,.F.);
#2568=EDGE_CURVE('',#1832,#1835,#291,.T.);
#2569=EDGE_CURVE('',#1837,#1838,#1183,.T.);
#2570=EDGE_CURVE('',#1834,#1837,#292,.F.);
#2571=EDGE_CURVE('',#1835,#1839,#293,.T.);
#2572=EDGE_CURVE('',#1839,#1838,#294,.T.);
#2573=EDGE_CURVE('',#1840,#1841,#1184,.T.);
#2574=EDGE_CURVE('',#1842,#1840,#295,.T.);
#2575=EDGE_CURVE('',#1837,#1842,#296,.F.);
#2576=EDGE_CURVE('',#1838,#1841,#297,.T.);
#2577=EDGE_CURVE('',#1843,#1844,#1185,.T.);
#2578=EDGE_CURVE('',#1845,#1843,#298,.F.);
#2579=EDGE_CURVE('',#1840,#1845,#299,.T.);
#2580=EDGE_CURVE('',#1841,#1846,#300,.T.);
#2581=EDGE_CURVE('',#1846,#1844,#301,.T.);
#2582=EDGE_CURVE('',#1847,#1848,#1186,.T.);
#2583=EDGE_CURVE('',#1843,#1847,#302,.F.);
#2584=EDGE_CURVE('',#1844,#1848,#303,.T.);
#2585=EDGE_CURVE('',#1849,#1850,#1187,.T.);
#2586=EDGE_CURVE('',#1851,#1849,#304,.T.);
#2587=EDGE_CURVE('',#1847,#1851,#305,.F.);
#2588=EDGE_CURVE('',#1848,#1852,#306,.T.);
#2589=EDGE_CURVE('',#1852,#1850,#307,.F.);
#2590=EDGE_CURVE('',#1853,#1854,#308,.T.);
#2591=EDGE_CURVE('',#1855,#1854,#1458,.T.);
#2592=EDGE_CURVE('',#1855,#1856,#309,.T.);
#2593=EDGE_CURVE('',#1856,#1857,#310,.T.);
#2594=EDGE_CURVE('',#1857,#1858,#311,.T.);
#2595=EDGE_CURVE('',#1858,#1859,#312,.T.);
#2596=EDGE_CURVE('',#1859,#1860,#313,.T.);
#2597=EDGE_CURVE('',#1860,#1861,#314,.T.);
#2598=EDGE_CURVE('',#1861,#1862,#315,.T.);
#2599=EDGE_CURVE('',#1862,#1863,#316,.T.);
#2600=EDGE_CURVE('',#1863,#1864,#317,.T.);
#2601=EDGE_CURVE('',#1864,#1865,#318,.T.);
#2602=EDGE_CURVE('',#1865,#1866,#319,.T.);
#2603=EDGE_CURVE('',#1866,#1867,#320,.T.);
#2604=EDGE_CURVE('',#1867,#1868,#321,.T.);
#2605=EDGE_CURVE('',#1868,#1869,#322,.T.);
#2606=EDGE_CURVE('',#1869,#1870,#323,.T.);
#2607=EDGE_CURVE('',#1870,#1871,#324,.T.);
#2608=EDGE_CURVE('',#1871,#1872,#325,.T.);
#2609=EDGE_CURVE('',#1872,#1873,#326,.T.);
#2610=EDGE_CURVE('',#1873,#1874,#327,.T.);
#2611=EDGE_CURVE('',#1874,#1875,#328,.T.);
#2612=EDGE_CURVE('',#1875,#1876,#329,.T.);
#2613=EDGE_CURVE('',#1876,#1877,#330,.T.);
#2614=EDGE_CURVE('',#1877,#1878,#331,.T.);
#2615=EDGE_CURVE('',#1878,#1879,#332,.T.);
#2616=EDGE_CURVE('',#1879,#1880,#333,.T.);
#2617=EDGE_CURVE('',#1880,#1881,#334,.T.);
#2618=EDGE_CURVE('',#1881,#1882,#335,.T.);
#2619=EDGE_CURVE('',#1882,#1883,#336,.T.);
#2620=EDGE_CURVE('',#1883,#1884,#337,.T.);
#2621=EDGE_CURVE('',#1884,#1885,#338,.T.);
#2622=EDGE_CURVE('',#1885,#1886,#339,.T.);
#2623=EDGE_CURVE('',#1886,#1887,#340,.T.);
#2624=EDGE_CURVE('',#1887,#1888,#341,.T.);
#2625=EDGE_CURVE('',#1888,#1889,#342,.T.);
#2626=EDGE_CURVE('',#1889,#1890,#343,.T.);
#2627=EDGE_CURVE('',#1890,#1891,#344,.T.);
#2628=EDGE_CURVE('',#1891,#1892,#345,.T.);
#2629=EDGE_CURVE('',#1892,#1893,#346,.T.);
#2630=EDGE_CURVE('',#1893,#1894,#347,.T.);
#2631=EDGE_CURVE('',#1894,#1895,#348,.T.);
#2632=EDGE_CURVE('',#1895,#1896,#349,.T.);
#2633=EDGE_CURVE('',#1896,#1897,#350,.T.);
#2634=EDGE_CURVE('',#1897,#1898,#351,.T.);
#2635=EDGE_CURVE('',#1898,#1899,#352,.T.);
#2636=EDGE_CURVE('',#1899,#1900,#353,.T.);
#2637=EDGE_CURVE('',#1900,#1901,#354,.T.);
#2638=EDGE_CURVE('',#1901,#1902,#355,.T.);
#2639=EDGE_CURVE('',#1902,#1903,#356,.T.);
#2640=EDGE_CURVE('',#1903,#1904,#357,.T.);
#2641=EDGE_CURVE('',#1904,#1905,#358,.T.);
#2642=EDGE_CURVE('',#1905,#1906,#359,.T.);
#2643=EDGE_CURVE('',#1906,#1907,#360,.T.);
#2644=EDGE_CURVE('',#1907,#1908,#361,.T.);
#2645=EDGE_CURVE('',#1908,#1909,#362,.T.);
#2646=EDGE_CURVE('',#1909,#1910,#363,.T.);
#2647=EDGE_CURVE('',#1910,#1911,#364,.T.);
#2648=EDGE_CURVE('',#1911,#1912,#365,.T.);
#2649=EDGE_CURVE('',#1912,#1913,#366,.T.);
#2650=EDGE_CURVE('',#1913,#1914,#367,.T.);
#2651=EDGE_CURVE('',#1914,#1915,#368,.T.);
#2652=EDGE_CURVE('',#1915,#1916,#369,.T.);
#2653=EDGE_CURVE('',#1916,#1917,#370,.T.);
#2654=EDGE_CURVE('',#1917,#1918,#371,.T.);
#2655=EDGE_CURVE('',#1918,#1919,#372,.T.);
#2656=EDGE_CURVE('',#1919,#1920,#373,.T.);
#2657=EDGE_CURVE('',#1920,#1921,#374,.T.);
#2658=EDGE_CURVE('',#1921,#1922,#375,.T.);
#2659=EDGE_CURVE('',#1922,#1923,#376,.T.);
#2660=EDGE_CURVE('',#1923,#1924,#377,.T.);
#2661=EDGE_CURVE('',#1924,#1925,#378,.T.);
#2662=EDGE_CURVE('',#1925,#1926,#379,.T.);
#2663=EDGE_CURVE('',#1926,#1927,#380,.T.);
#2664=EDGE_CURVE('',#1927,#1928,#381,.T.);
#2665=EDGE_CURVE('',#1928,#1929,#382,.T.);
#2666=EDGE_CURVE('',#1929,#1930,#383,.T.);
#2667=EDGE_CURVE('',#1930,#1931,#384,.T.);
#2668=EDGE_CURVE('',#1931,#1932,#385,.T.);
#2669=EDGE_CURVE('',#1932,#1933,#386,.T.);
#2670=EDGE_CURVE('',#1933,#1934,#387,.T.);
#2671=EDGE_CURVE('',#1934,#1935,#388,.T.);
#2672=EDGE_CURVE('',#1935,#1936,#389,.T.);
#2673=EDGE_CURVE('',#1936,#1937,#390,.T.);
#2674=EDGE_CURVE('',#1937,#1938,#391,.T.);
#2675=EDGE_CURVE('',#1938,#1939,#392,.T.);
#2676=EDGE_CURVE('',#1939,#1940,#393,.T.);
#2677=EDGE_CURVE('',#1941,#1940,#1459,.F.);
#2678=EDGE_CURVE('',#1941,#1942,#394,.T.);
#2679=EDGE_CURVE('',#1942,#1943,#395,.T.);
#2680=EDGE_CURVE('',#1943,#1944,#396,.T.);
#2681=EDGE_CURVE('',#1944,#1945,#397,.T.);
#2682=EDGE_CURVE('',#1945,#1946,#398,.T.);
#2683=EDGE_CURVE('',#1946,#1947,#399,.T.);
#2684=EDGE_CURVE('',#1947,#1948,#400,.T.);
#2685=EDGE_CURVE('',#1948,#1949,#401,.T.);
#2686=EDGE_CURVE('',#1949,#1950,#402,.T.);
#2687=EDGE_CURVE('',#1950,#1951,#403,.T.);
#2688=EDGE_CURVE('',#1951,#1952,#404,.T.);
#2689=EDGE_CURVE('',#1952,#1953,#405,.T.);
#2690=EDGE_CURVE('',#1953,#1954,#406,.T.);
#2691=EDGE_CURVE('',#1954,#1955,#407,.T.);
#2692=EDGE_CURVE('',#1955,#1956,#408,.T.);
#2693=EDGE_CURVE('',#1956,#1957,#409,.T.);
#2694=EDGE_CURVE('',#1957,#1958,#410,.T.);
#2695=EDGE_CURVE('',#1958,#1959,#411,.T.);
#2696=EDGE_CURVE('',#1959,#1960,#412,.T.);
#2697=EDGE_CURVE('',#1960,#1961,#413,.T.);
#2698=EDGE_CURVE('',#1961,#1962,#414,.T.);
#2699=EDGE_CURVE('',#1962,#1963,#415,.T.);
#2700=EDGE_CURVE('',#1963,#1964,#416,.T.);
#2701=EDGE_CURVE('',#1964,#1965,#417,.T.);
#2702=EDGE_CURVE('',#1965,#1966,#418,.T.);
#2703=EDGE_CURVE('',#1966,#1967,#419,.T.);
#2704=EDGE_CURVE('',#1967,#1968,#420,.T.);
#2705=EDGE_CURVE('',#1968,#1969,#421,.T.);
#2706=EDGE_CURVE('',#1969,#1970,#422,.T.);
#2707=EDGE_CURVE('',#1970,#1971,#423,.T.);
#2708=EDGE_CURVE('',#1971,#1972,#424,.T.);
#2709=EDGE_CURVE('',#1972,#1973,#425,.T.);
#2710=EDGE_CURVE('',#1973,#1974,#426,.T.);
#2711=EDGE_CURVE('',#1974,#1975,#427,.T.);
#2712=EDGE_CURVE('',#1975,#1976,#428,.T.);
#2713=EDGE_CURVE('',#1976,#1977,#429,.T.);
#2714=EDGE_CURVE('',#1977,#1978,#430,.T.);
#2715=EDGE_CURVE('',#1978,#1979,#431,.T.);
#2716=EDGE_CURVE('',#1979,#1980,#432,.T.);
#2717=EDGE_CURVE('',#1980,#1981,#433,.T.);
#2718=EDGE_CURVE('',#1981,#1982,#434,.T.);
#2719=EDGE_CURVE('',#1982,#1983,#435,.T.);
#2720=EDGE_CURVE('',#1983,#1984,#436,.T.);
#2721=EDGE_CURVE('',#1984,#1985,#437,.T.);
#2722=EDGE_CURVE('',#1985,#1986,#438,.T.);
#2723=EDGE_CURVE('',#1986,#1987,#439,.T.);
#2724=EDGE_CURVE('',#1987,#1988,#440,.T.);
#2725=EDGE_CURVE('',#1988,#1989,#441,.T.);
#2726=EDGE_CURVE('',#1989,#1990,#442,.T.);
#2727=EDGE_CURVE('',#1990,#1991,#443,.T.);
#2728=EDGE_CURVE('',#1991,#1992,#444,.T.);
#2729=EDGE_CURVE('',#1992,#1993,#445,.T.);
#2730=EDGE_CURVE('',#1993,#1994,#446,.T.);
#2731=EDGE_CURVE('',#1994,#1995,#447,.T.);
#2732=EDGE_CURVE('',#1995,#1996,#448,.T.);
#2733=EDGE_CURVE('',#1996,#1997,#449,.T.);
#2734=EDGE_CURVE('',#1997,#1998,#450,.T.);
#2735=EDGE_CURVE('',#1998,#1999,#451,.T.);
#2736=EDGE_CURVE('',#1999,#2000,#452,.T.);
#2737=EDGE_CURVE('',#2000,#2001,#453,.T.);
#2738=EDGE_CURVE('',#2001,#2002,#454,.T.);
#2739=EDGE_CURVE('',#2002,#2003,#455,.T.);
#2740=EDGE_CURVE('',#2003,#2004,#456,.T.);
#2741=EDGE_CURVE('',#2004,#2005,#457,.T.);
#2742=EDGE_CURVE('',#2005,#2006,#458,.T.);
#2743=EDGE_CURVE('',#2006,#2007,#459,.T.);
#2744=EDGE_CURVE('',#2007,#2008,#460,.T.);
#2745=EDGE_CURVE('',#2008,#2009,#461,.T.);
#2746=EDGE_CURVE('',#2009,#2010,#462,.T.);
#2747=EDGE_CURVE('',#2010,#2011,#463,.T.);
#2748=EDGE_CURVE('',#2011,#2012,#464,.T.);
#2749=EDGE_CURVE('',#2012,#2013,#465,.T.);
#2750=EDGE_CURVE('',#2013,#2014,#466,.T.);
#2751=EDGE_CURVE('',#2014,#2015,#467,.T.);
#2752=EDGE_CURVE('',#2015,#2016,#468,.T.);
#2753=EDGE_CURVE('',#2016,#2017,#469,.T.);
#2754=EDGE_CURVE('',#2017,#2018,#470,.T.);
#2755=EDGE_CURVE('',#2018,#2019,#471,.T.);
#2756=EDGE_CURVE('',#2019,#2020,#472,.T.);
#2757=EDGE_CURVE('',#2020,#2021,#473,.T.);
#2758=EDGE_CURVE('',#2021,#2022,#474,.T.);
#2759=EDGE_CURVE('',#2022,#2023,#475,.T.);
#2760=EDGE_CURVE('',#2023,#2024,#476,.T.);
#2761=EDGE_CURVE('',#2024,#1853,#477,.T.);
#2762=EDGE_CURVE('',#1850,#2025,#478,.F.);
#2763=EDGE_CURVE('',#2026,#2025,#1460,.T.);
#2764=EDGE_CURVE('',#2027,#2026,#479,.T.);
#2765=EDGE_CURVE('',#1849,#2027,#480,.T.);
#2766=EDGE_CURVE('',#1940,#2026,#481,.T.);
#2767=EDGE_CURVE('',#1594,#1855,#482,.T.);
#2768=EDGE_CURVE('',#2028,#1941,#483,.T.);
#2769=EDGE_CURVE('',#2025,#2028,#484,.T.);
#2770=EDGE_CURVE('',#1854,#1595,#485,.T.);
#3205=ORIENTED_EDGE('',*,*,#2246,.F.);
#3206=ORIENTED_EDGE('',*,*,#2247,.F.);
#3207=ORIENTED_EDGE('',*,*,#2248,.F.);
#3208=ORIENTED_EDGE('',*,*,#2249,.T.);
#3209=ORIENTED_EDGE('',*,*,#2250,.F.);
#3210=ORIENTED_EDGE('',*,*,#2251,.F.);
#3211=ORIENTED_EDGE('',*,*,#2252,.F.);
#3212=ORIENTED_EDGE('',*,*,#2246,.T.);
#3213=ORIENTED_EDGE('',*,*,#2253,.T.);
#3214=ORIENTED_EDGE('',*,*,#2254,.T.);
#3215=ORIENTED_EDGE('',*,*,#2255,.F.);
#3216=ORIENTED_EDGE('',*,*,#2256,.F.);
#3217=ORIENTED_EDGE('',*,*,#2250,.T.);
#3218=ORIENTED_EDGE('',*,*,#2257,.T.);
#3219=ORIENTED_EDGE('',*,*,#2258,.F.);
#3220=ORIENTED_EDGE('',*,*,#2259,.F.);
#3221=ORIENTED_EDGE('',*,*,#2260,.F.);
#3222=ORIENTED_EDGE('',*,*,#2255,.T.);
#3223=ORIENTED_EDGE('',*,*,#2261,.T.);
#3224=ORIENTED_EDGE('',*,*,#2262,.T.);
#3225=ORIENTED_EDGE('',*,*,#2263,.F.);
#3226=ORIENTED_EDGE('',*,*,#2264,.F.);
#3227=ORIENTED_EDGE('',*,*,#2258,.T.);
#3228=ORIENTED_EDGE('',*,*,#2265,.T.);
#3229=ORIENTED_EDGE('',*,*,#2266,.F.);
#3230=ORIENTED_EDGE('',*,*,#2267,.F.);
#3231=ORIENTED_EDGE('',*,*,#2268,.F.);
#3232=ORIENTED_EDGE('',*,*,#2263,.T.);
#3233=ORIENTED_EDGE('',*,*,#2269,.T.);
#3234=ORIENTED_EDGE('',*,*,#2270,.T.);
#3235=ORIENTED_EDGE('',*,*,#2271,.F.);
#3236=ORIENTED_EDGE('',*,*,#2272,.F.);
#3237=ORIENTED_EDGE('',*,*,#2266,.T.);
#3238=ORIENTED_EDGE('',*,*,#2273,.T.);
#3239=ORIENTED_EDGE('',*,*,#2274,.F.);
#3240=ORIENTED_EDGE('',*,*,#2275,.F.);
#3241=ORIENTED_EDGE('',*,*,#2276,.F.);
#3242=ORIENTED_EDGE('',*,*,#2271,.T.);
#3243=ORIENTED_EDGE('',*,*,#2277,.T.);
#3244=ORIENTED_EDGE('',*,*,#2278,.T.);
#3245=ORIENTED_EDGE('',*,*,#2279,.F.);
#3246=ORIENTED_EDGE('',*,*,#2280,.F.);
#3247=ORIENTED_EDGE('',*,*,#2274,.T.);
#3248=ORIENTED_EDGE('',*,*,#2281,.T.);
#3249=ORIENTED_EDGE('',*,*,#2282,.F.);
#3250=ORIENTED_EDGE('',*,*,#2283,.F.);
#3251=ORIENTED_EDGE('',*,*,#2284,.F.);
#3252=ORIENTED_EDGE('',*,*,#2279,.T.);
#3253=ORIENTED_EDGE('',*,*,#2285,.T.);
#3254=ORIENTED_EDGE('',*,*,#2286,.T.);
#3255=ORIENTED_EDGE('',*,*,#2287,.F.);
#3256=ORIENTED_EDGE('',*,*,#2288,.F.);
#3257=ORIENTED_EDGE('',*,*,#2282,.T.);
#3258=ORIENTED_EDGE('',*,*,#2289,.T.);
#3259=ORIENTED_EDGE('',*,*,#2290,.F.);
#3260=ORIENTED_EDGE('',*,*,#2291,.F.);
#3261=ORIENTED_EDGE('',*,*,#2292,.F.);
#3262=ORIENTED_EDGE('',*,*,#2287,.T.);
#3263=ORIENTED_EDGE('',*,*,#2293,.T.);
#3264=ORIENTED_EDGE('',*,*,#2294,.T.);
#3265=ORIENTED_EDGE('',*,*,#2295,.F.);
#3266=ORIENTED_EDGE('',*,*,#2296,.F.);
#3267=ORIENTED_EDGE('',*,*,#2290,.T.);
#3268=ORIENTED_EDGE('',*,*,#2297,.T.);
#3269=ORIENTED_EDGE('',*,*,#2298,.F.);
#3270=ORIENTED_EDGE('',*,*,#2299,.F.);
#3271=ORIENTED_EDGE('',*,*,#2300,.F.);
#3272=ORIENTED_EDGE('',*,*,#2295,.T.);
#3273=ORIENTED_EDGE('',*,*,#2301,.T.);
#3274=ORIENTED_EDGE('',*,*,#2302,.T.);
#3275=ORIENTED_EDGE('',*,*,#2303,.F.);
#3276=ORIENTED_EDGE('',*,*,#2304,.F.);
#3277=ORIENTED_EDGE('',*,*,#2298,.T.);
#3278=ORIENTED_EDGE('',*,*,#2305,.T.);
#3279=ORIENTED_EDGE('',*,*,#2306,.F.);
#3280=ORIENTED_EDGE('',*,*,#2307,.F.);
#3281=ORIENTED_EDGE('',*,*,#2308,.F.);
#3282=ORIENTED_EDGE('',*,*,#2303,.T.);
#3283=ORIENTED_EDGE('',*,*,#2309,.T.);
#3284=ORIENTED_EDGE('',*,*,#2310,.T.);
#3285=ORIENTED_EDGE('',*,*,#2311,.F.);
#3286=ORIENTED_EDGE('',*,*,#2312,.F.);
#3287=ORIENTED_EDGE('',*,*,#2306,.T.);
#3288=ORIENTED_EDGE('',*,*,#2313,.T.);
#3289=ORIENTED_EDGE('',*,*,#2314,.T.);
#3290=ORIENTED_EDGE('',*,*,#2315,.F.);
#3291=ORIENTED_EDGE('',*,*,#2316,.F.);
#3292=ORIENTED_EDGE('',*,*,#2317,.F.);
#3293=ORIENTED_EDGE('',*,*,#2311,.T.);
#3294=ORIENTED_EDGE('',*,*,#2318,.T.);
#3295=ORIENTED_EDGE('',*,*,#2319,.F.);
#3296=ORIENTED_EDGE('',*,*,#2320,.F.);
#3297=ORIENTED_EDGE('',*,*,#2315,.T.);
#3298=ORIENTED_EDGE('',*,*,#2321,.T.);
#3299=ORIENTED_EDGE('',*,*,#2322,.T.);
#3300=ORIENTED_EDGE('',*,*,#2323,.F.);
#3301=ORIENTED_EDGE('',*,*,#2324,.F.);
#3302=ORIENTED_EDGE('',*,*,#2325,.F.);
#3303=ORIENTED_EDGE('',*,*,#2319,.T.);
#3304=ORIENTED_EDGE('',*,*,#2326,.T.);
#3305=ORIENTED_EDGE('',*,*,#2327,.F.);
#3306=ORIENTED_EDGE('',*,*,#2328,.F.);
#3307=ORIENTED_EDGE('',*,*,#2323,.T.);
#3308=ORIENTED_EDGE('',*,*,#2329,.T.);
#3309=ORIENTED_EDGE('',*,*,#2330,.T.);
#3310=ORIENTED_EDGE('',*,*,#2331,.F.);
#3311=ORIENTED_EDGE('',*,*,#2332,.F.);
#3312=ORIENTED_EDGE('',*,*,#2333,.F.);
#3313=ORIENTED_EDGE('',*,*,#2327,.T.);
#3314=ORIENTED_EDGE('',*,*,#2334,.T.);
#3315=ORIENTED_EDGE('',*,*,#2335,.F.);
#3316=ORIENTED_EDGE('',*,*,#2336,.F.);
#3317=ORIENTED_EDGE('',*,*,#2331,.T.);
#3318=ORIENTED_EDGE('',*,*,#2337,.T.);
#3319=ORIENTED_EDGE('',*,*,#2338,.T.);
#3320=ORIENTED_EDGE('',*,*,#2339,.F.);
#3321=ORIENTED_EDGE('',*,*,#2340,.F.);
#3322=ORIENTED_EDGE('',*,*,#2341,.F.);
#3323=ORIENTED_EDGE('',*,*,#2335,.T.);
#3324=ORIENTED_EDGE('',*,*,#2342,.T.);
#3325=ORIENTED_EDGE('',*,*,#2343,.F.);
#3326=ORIENTED_EDGE('',*,*,#2344,.F.);
#3327=ORIENTED_EDGE('',*,*,#2339,.T.);
#3328=ORIENTED_EDGE('',*,*,#2345,.T.);
#3329=ORIENTED_EDGE('',*,*,#2346,.T.);
#3330=ORIENTED_EDGE('',*,*,#2347,.F.);
#3331=ORIENTED_EDGE('',*,*,#2348,.F.);
#3332=ORIENTED_EDGE('',*,*,#2349,.F.);
#3333=ORIENTED_EDGE('',*,*,#2343,.T.);
#3334=ORIENTED_EDGE('',*,*,#2350,.T.);
#3335=ORIENTED_EDGE('',*,*,#2351,.F.);
#3336=ORIENTED_EDGE('',*,*,#2352,.F.);
#3337=ORIENTED_EDGE('',*,*,#2347,.T.);
#3338=ORIENTED_EDGE('',*,*,#2353,.T.);
#3339=ORIENTED_EDGE('',*,*,#2354,.T.);
#3340=ORIENTED_EDGE('',*,*,#2355,.F.);
#3341=ORIENTED_EDGE('',*,*,#2356,.F.);
#3342=ORIENTED_EDGE('',*,*,#2357,.F.);
#3343=ORIENTED_EDGE('',*,*,#2351,.T.);
#3344=ORIENTED_EDGE('',*,*,#2358,.T.);
#3345=ORIENTED_EDGE('',*,*,#2359,.F.);
#3346=ORIENTED_EDGE('',*,*,#2360,.F.);
#3347=ORIENTED_EDGE('',*,*,#2355,.T.);
#3348=ORIENTED_EDGE('',*,*,#2361,.T.);
#3349=ORIENTED_EDGE('',*,*,#2362,.T.);
#3350=ORIENTED_EDGE('',*,*,#2363,.F.);
#3351=ORIENTED_EDGE('',*,*,#2364,.F.);
#3352=ORIENTED_EDGE('',*,*,#2365,.F.);
#3353=ORIENTED_EDGE('',*,*,#2359,.T.);
#3354=ORIENTED_EDGE('',*,*,#2366,.T.);
#3355=ORIENTED_EDGE('',*,*,#2367,.F.);
#3356=ORIENTED_EDGE('',*,*,#2368,.F.);
#3357=ORIENTED_EDGE('',*,*,#2363,.T.);
#3358=ORIENTED_EDGE('',*,*,#2369,.T.);
#3359=ORIENTED_EDGE('',*,*,#2370,.T.);
#3360=ORIENTED_EDGE('',*,*,#2371,.F.);
#3361=ORIENTED_EDGE('',*,*,#2372,.F.);
#3362=ORIENTED_EDGE('',*,*,#2373,.F.);
#3363=ORIENTED_EDGE('',*,*,#2367,.T.);
#3364=ORIENTED_EDGE('',*,*,#2374,.T.);
#3365=ORIENTED_EDGE('',*,*,#2375,.F.);
#3366=ORIENTED_EDGE('',*,*,#2376,.F.);
#3367=ORIENTED_EDGE('',*,*,#2371,.T.);
#3368=ORIENTED_EDGE('',*,*,#2377,.T.);
#3369=ORIENTED_EDGE('',*,*,#2378,.T.);
#3370=ORIENTED_EDGE('',*,*,#2379,.F.);
#3371=ORIENTED_EDGE('',*,*,#2380,.F.);
#3372=ORIENTED_EDGE('',*,*,#2381,.F.);
#3373=ORIENTED_EDGE('',*,*,#2375,.T.);
#3374=ORIENTED_EDGE('',*,*,#2382,.T.);
#3375=ORIENTED_EDGE('',*,*,#2383,.F.);
#3376=ORIENTED_EDGE('',*,*,#2384,.F.);
#3377=ORIENTED_EDGE('',*,*,#2379,.T.);
#3378=ORIENTED_EDGE('',*,*,#2385,.T.);
#3379=ORIENTED_EDGE('',*,*,#2386,.T.);
#3380=ORIENTED_EDGE('',*,*,#2387,.F.);
#3381=ORIENTED_EDGE('',*,*,#2388,.F.);
#3382=ORIENTED_EDGE('',*,*,#2389,.F.);
#3383=ORIENTED_EDGE('',*,*,#2383,.T.);
#3384=ORIENTED_EDGE('',*,*,#2390,.T.);
#3385=ORIENTED_EDGE('',*,*,#2391,.F.);
#3386=ORIENTED_EDGE('',*,*,#2392,.F.);
#3387=ORIENTED_EDGE('',*,*,#2387,.T.);
#3388=ORIENTED_EDGE('',*,*,#2393,.T.);
#3389=ORIENTED_EDGE('',*,*,#2394,.T.);
#3390=ORIENTED_EDGE('',*,*,#2395,.F.);
#3391=ORIENTED_EDGE('',*,*,#2396,.F.);
#3392=ORIENTED_EDGE('',*,*,#2397,.F.);
#3393=ORIENTED_EDGE('',*,*,#2391,.T.);
#3394=ORIENTED_EDGE('',*,*,#2398,.T.);
#3395=ORIENTED_EDGE('',*,*,#2399,.T.);
#3396=ORIENTED_EDGE('',*,*,#2400,.F.);
#3397=ORIENTED_EDGE('',*,*,#2401,.F.);
#3398=ORIENTED_EDGE('',*,*,#2395,.T.);
#3399=ORIENTED_EDGE('',*,*,#2402,.T.);
#3400=ORIENTED_EDGE('',*,*,#2403,.F.);
#3401=ORIENTED_EDGE('',*,*,#2404,.F.);
#3402=ORIENTED_EDGE('',*,*,#2405,.F.);
#3403=ORIENTED_EDGE('',*,*,#2400,.T.);
#3404=ORIENTED_EDGE('',*,*,#2406,.T.);
#3405=ORIENTED_EDGE('',*,*,#2407,.T.);
#3406=ORIENTED_EDGE('',*,*,#2408,.F.);
#3407=ORIENTED_EDGE('',*,*,#2409,.F.);
#3408=ORIENTED_EDGE('',*,*,#2403,.T.);
#3409=ORIENTED_EDGE('',*,*,#2410,.T.);
#3410=ORIENTED_EDGE('',*,*,#2411,.T.);
#3411=ORIENTED_EDGE('',*,*,#2412,.F.);
#3412=ORIENTED_EDGE('',*,*,#2413,.F.);
#3413=ORIENTED_EDGE('',*,*,#2414,.F.);
#3414=ORIENTED_EDGE('',*,*,#2408,.T.);
#3415=ORIENTED_EDGE('',*,*,#2415,.T.);
#3416=ORIENTED_EDGE('',*,*,#2416,.F.);
#3417=ORIENTED_EDGE('',*,*,#2417,.F.);
#3418=ORIENTED_EDGE('',*,*,#2412,.T.);
#3419=ORIENTED_EDGE('',*,*,#2418,.T.);
#3420=ORIENTED_EDGE('',*,*,#2419,.T.);
#3421=ORIENTED_EDGE('',*,*,#2420,.F.);
#3422=ORIENTED_EDGE('',*,*,#2421,.F.);
#3423=ORIENTED_EDGE('',*,*,#2422,.F.);
#3424=ORIENTED_EDGE('',*,*,#2416,.T.);
#3425=ORIENTED_EDGE('',*,*,#2423,.T.);
#3426=ORIENTED_EDGE('',*,*,#2424,.F.);
#3427=ORIENTED_EDGE('',*,*,#2425,.F.);
#3428=ORIENTED_EDGE('',*,*,#2426,.F.);
#3429=ORIENTED_EDGE('',*,*,#2420,.T.);
#3430=ORIENTED_EDGE('',*,*,#2427,.T.);
#3431=ORIENTED_EDGE('',*,*,#2428,.T.);
#3432=ORIENTED_EDGE('',*,*,#2429,.F.);
#3433=ORIENTED_EDGE('',*,*,#2430,.F.);
#3434=ORIENTED_EDGE('',*,*,#2424,.T.);
#3435=ORIENTED_EDGE('',*,*,#2431,.T.);
#3436=ORIENTED_EDGE('',*,*,#2432,.T.);
#3437=ORIENTED_EDGE('',*,*,#2433,.F.);
#3438=ORIENTED_EDGE('',*,*,#2434,.F.);
#3439=ORIENTED_EDGE('',*,*,#2435,.F.);
#3440=ORIENTED_EDGE('',*,*,#2429,.T.);
#3441=ORIENTED_EDGE('',*,*,#2436,.T.);
#3442=ORIENTED_EDGE('',*,*,#2437,.F.);
#3443=ORIENTED_EDGE('',*,*,#2438,.F.);
#3444=ORIENTED_EDGE('',*,*,#2433,.T.);
#3445=ORIENTED_EDGE('',*,*,#2439,.T.);
#3446=ORIENTED_EDGE('',*,*,#2440,.T.);
#3447=ORIENTED_EDGE('',*,*,#2441,.F.);
#3448=ORIENTED_EDGE('',*,*,#2442,.F.);
#3449=ORIENTED_EDGE('',*,*,#2443,.F.);
#3450=ORIENTED_EDGE('',*,*,#2437,.T.);
#3451=ORIENTED_EDGE('',*,*,#2444,.T.);
#3452=ORIENTED_EDGE('',*,*,#2445,.F.);
#3453=ORIENTED_EDGE('',*,*,#2446,.F.);
#3454=ORIENTED_EDGE('',*,*,#2441,.T.);
#3455=ORIENTED_EDGE('',*,*,#2447,.T.);
#3456=ORIENTED_EDGE('',*,*,#2448,.T.);
#3457=ORIENTED_EDGE('',*,*,#2449,.F.);
#3458=ORIENTED_EDGE('',*,*,#2450,.F.);
#3459=ORIENTED_EDGE('',*,*,#2451,.F.);
#3460=ORIENTED_EDGE('',*,*,#2445,.T.);
#3461=ORIENTED_EDGE('',*,*,#2452,.T.);
#3462=ORIENTED_EDGE('',*,*,#2453,.T.);
#3463=ORIENTED_EDGE('',*,*,#2454,.F.);
#3464=ORIENTED_EDGE('',*,*,#2455,.F.);
#3465=ORIENTED_EDGE('',*,*,#2456,.F.);
#3466=ORIENTED_EDGE('',*,*,#2449,.T.);
#3467=ORIENTED_EDGE('',*,*,#2457,.T.);
#3468=ORIENTED_EDGE('',*,*,#2458,.F.);
#3469=ORIENTED_EDGE('',*,*,#2459,.F.);
#3470=ORIENTED_EDGE('',*,*,#2454,.T.);
#3471=ORIENTED_EDGE('',*,*,#2460,.T.);
#3472=ORIENTED_EDGE('',*,*,#2461,.T.);
#3473=ORIENTED_EDGE('',*,*,#2462,.F.);
#3474=ORIENTED_EDGE('',*,*,#2463,.F.);
#3475=ORIENTED_EDGE('',*,*,#2464,.F.);
#3476=ORIENTED_EDGE('',*,*,#2458,.T.);
#3477=ORIENTED_EDGE('',*,*,#2465,.T.);
#3478=ORIENTED_EDGE('',*,*,#2466,.T.);
#3479=ORIENTED_EDGE('',*,*,#2467,.F.);
#3480=ORIENTED_EDGE('',*,*,#2468,.F.);
#3481=ORIENTED_EDGE('',*,*,#2462,.T.);
#3482=ORIENTED_EDGE('',*,*,#2469,.T.);
#3483=ORIENTED_EDGE('',*,*,#2470,.F.);
#3484=ORIENTED_EDGE('',*,*,#2471,.F.);
#3485=ORIENTED_EDGE('',*,*,#2472,.F.);
#3486=ORIENTED_EDGE('',*,*,#2467,.T.);
#3487=ORIENTED_EDGE('',*,*,#2473,.T.);
#3488=ORIENTED_EDGE('',*,*,#2474,.T.);
#3489=ORIENTED_EDGE('',*,*,#2475,.F.);
#3490=ORIENTED_EDGE('',*,*,#2476,.F.);
#3491=ORIENTED_EDGE('',*,*,#2470,.T.);
#3492=ORIENTED_EDGE('',*,*,#2477,.T.);
#3493=ORIENTED_EDGE('',*,*,#2478,.T.);
#3494=ORIENTED_EDGE('',*,*,#2479,.F.);
#3495=ORIENTED_EDGE('',*,*,#2480,.F.);
#3496=ORIENTED_EDGE('',*,*,#2481,.F.);
#3497=ORIENTED_EDGE('',*,*,#2475,.T.);
#3498=ORIENTED_EDGE('',*,*,#2482,.T.);
#3499=ORIENTED_EDGE('',*,*,#2483,.F.);
#3500=ORIENTED_EDGE('',*,*,#2484,.F.);
#3501=ORIENTED_EDGE('',*,*,#2479,.T.);
#3502=ORIENTED_EDGE('',*,*,#2485,.T.);
#3503=ORIENTED_EDGE('',*,*,#2486,.T.);
#3504=ORIENTED_EDGE('',*,*,#2487,.F.);
#3505=ORIENTED_EDGE('',*,*,#2488,.F.);
#3506=ORIENTED_EDGE('',*,*,#2489,.F.);
#3507=ORIENTED_EDGE('',*,*,#2483,.T.);
#3508=ORIENTED_EDGE('',*,*,#2490,.T.);
#3509=ORIENTED_EDGE('',*,*,#2491,.F.);
#3510=ORIENTED_EDGE('',*,*,#2492,.F.);
#3511=ORIENTED_EDGE('',*,*,#2487,.T.);
#3512=ORIENTED_EDGE('',*,*,#2493,.T.);
#3513=ORIENTED_EDGE('',*,*,#2494,.T.);
#3514=ORIENTED_EDGE('',*,*,#2495,.F.);
#3515=ORIENTED_EDGE('',*,*,#2496,.F.);
#3516=ORIENTED_EDGE('',*,*,#2497,.F.);
#3517=ORIENTED_EDGE('',*,*,#2491,.T.);
#3518=ORIENTED_EDGE('',*,*,#2498,.T.);
#3519=ORIENTED_EDGE('',*,*,#2499,.F.);
#3520=ORIENTED_EDGE('',*,*,#2500,.F.);
#3521=ORIENTED_EDGE('',*,*,#2495,.T.);
#3522=ORIENTED_EDGE('',*,*,#2501,.T.);
#3523=ORIENTED_EDGE('',*,*,#2502,.T.);
#3524=ORIENTED_EDGE('',*,*,#2503,.F.);
#3525=ORIENTED_EDGE('',*,*,#2504,.F.);
#3526=ORIENTED_EDGE('',*,*,#2505,.F.);
#3527=ORIENTED_EDGE('',*,*,#2499,.T.);
#3528=ORIENTED_EDGE('',*,*,#2506,.T.);
#3529=ORIENTED_EDGE('',*,*,#2507,.F.);
#3530=ORIENTED_EDGE('',*,*,#2508,.F.);
#3531=ORIENTED_EDGE('',*,*,#2503,.T.);
#3532=ORIENTED_EDGE('',*,*,#2509,.T.);
#3533=ORIENTED_EDGE('',*,*,#2510,.T.);
#3534=ORIENTED_EDGE('',*,*,#2511,.F.);
#3535=ORIENTED_EDGE('',*,*,#2512,.F.);
#3536=ORIENTED_EDGE('',*,*,#2513,.F.);
#3537=ORIENTED_EDGE('',*,*,#2507,.T.);
#3538=ORIENTED_EDGE('',*,*,#2514,.T.);
#3539=ORIENTED_EDGE('',*,*,#2515,.F.);
#3540=ORIENTED_EDGE('',*,*,#2516,.F.);
#3541=ORIENTED_EDGE('',*,*,#2511,.T.);
#3542=ORIENTED_EDGE('',*,*,#2517,.T.);
#3543=ORIENTED_EDGE('',*,*,#2518,.T.);
#3544=ORIENTED_EDGE('',*,*,#2519,.F.);
#3545=ORIENTED_EDGE('',*,*,#2520,.F.);
#3546=ORIENTED_EDGE('',*,*,#2521,.F.);
#3547=ORIENTED_EDGE('',*,*,#2515,.T.);
#3548=ORIENTED_EDGE('',*,*,#2522,.T.);
#3549=ORIENTED_EDGE('',*,*,#2523,.F.);
#3550=ORIENTED_EDGE('',*,*,#2524,.F.);
#3551=ORIENTED_EDGE('',*,*,#2519,.T.);
#3552=ORIENTED_EDGE('',*,*,#2525,.T.);
#3553=ORIENTED_EDGE('',*,*,#2526,.T.);
#3554=ORIENTED_EDGE('',*,*,#2527,.F.);
#3555=ORIENTED_EDGE('',*,*,#2528,.F.);
#3556=ORIENTED_EDGE('',*,*,#2529,.F.);
#3557=ORIENTED_EDGE('',*,*,#2523,.T.);
#3558=ORIENTED_EDGE('',*,*,#2530,.T.);
#3559=ORIENTED_EDGE('',*,*,#2531,.F.);
#3560=ORIENTED_EDGE('',*,*,#2532,.F.);
#3561=ORIENTED_EDGE('',*,*,#2533,.F.);
#3562=ORIENTED_EDGE('',*,*,#2527,.T.);
#3563=ORIENTED_EDGE('',*,*,#2534,.T.);
#3564=ORIENTED_EDGE('',*,*,#2535,.T.);
#3565=ORIENTED_EDGE('',*,*,#2536,.F.);
#3566=ORIENTED_EDGE('',*,*,#2537,.F.);
#3567=ORIENTED_EDGE('',*,*,#2538,.F.);
#3568=ORIENTED_EDGE('',*,*,#2531,.T.);
#3569=ORIENTED_EDGE('',*,*,#2539,.T.);
#3570=ORIENTED_EDGE('',*,*,#2540,.F.);
#3571=ORIENTED_EDGE('',*,*,#2541,.F.);
#3572=ORIENTED_EDGE('',*,*,#2536,.T.);
#3573=ORIENTED_EDGE('',*,*,#2542,.T.);
#3574=ORIENTED_EDGE('',*,*,#2543,.T.);
#3575=ORIENTED_EDGE('',*,*,#2544,.F.);
#3576=ORIENTED_EDGE('',*,*,#2545,.F.);
#3577=ORIENTED_EDGE('',*,*,#2546,.F.);
#3578=ORIENTED_EDGE('',*,*,#2540,.T.);
#3579=ORIENTED_EDGE('',*,*,#2547,.T.);
#3580=ORIENTED_EDGE('',*,*,#2548,.T.);
#3581=ORIENTED_EDGE('',*,*,#2549,.F.);
#3582=ORIENTED_EDGE('',*,*,#2550,.F.);
#3583=ORIENTED_EDGE('',*,*,#2551,.F.);
#3584=ORIENTED_EDGE('',*,*,#2544,.T.);
#3585=ORIENTED_EDGE('',*,*,#2552,.T.);
#3586=ORIENTED_EDGE('',*,*,#2553,.F.);
#3587=ORIENTED_EDGE('',*,*,#2554,.F.);
#3588=ORIENTED_EDGE('',*,*,#2549,.T.);
#3589=ORIENTED_EDGE('',*,*,#2555,.T.);
#3590=ORIENTED_EDGE('',*,*,#2556,.T.);
#3591=ORIENTED_EDGE('',*,*,#2557,.F.);
#3592=ORIENTED_EDGE('',*,*,#2558,.F.);
#3593=ORIENTED_EDGE('',*,*,#2559,.F.);
#3594=ORIENTED_EDGE('',*,*,#2553,.T.);
#3595=ORIENTED_EDGE('',*,*,#2560,.T.);
#3596=ORIENTED_EDGE('',*,*,#2561,.F.);
#3597=ORIENTED_EDGE('',*,*,#2562,.F.);
#3598=ORIENTED_EDGE('',*,*,#2557,.T.);
#3599=ORIENTED_EDGE('',*,*,#2563,.T.);
#3600=ORIENTED_EDGE('',*,*,#2564,.T.);
#3601=ORIENTED_EDGE('',*,*,#2565,.F.);
#3602=ORIENTED_EDGE('',*,*,#2566,.F.);
#3603=ORIENTED_EDGE('',*,*,#2567,.F.);
#3604=ORIENTED_EDGE('',*,*,#2561,.T.);
#3605=ORIENTED_EDGE('',*,*,#2568,.T.);
#3606=ORIENTED_EDGE('',*,*,#2569,.F.);
#3607=ORIENTED_EDGE('',*,*,#2570,.F.);
#3608=ORIENTED_EDGE('',*,*,#2565,.T.);
#3609=ORIENTED_EDGE('',*,*,#2571,.T.);
#3610=ORIENTED_EDGE('',*,*,#2572,.T.);
#3611=ORIENTED_EDGE('',*,*,#2573,.F.);
#3612=ORIENTED_EDGE('',*,*,#2574,.F.);
#3613=ORIENTED_EDGE('',*,*,#2575,.F.);
#3614=ORIENTED_EDGE('',*,*,#2569,.T.);
#3615=ORIENTED_EDGE('',*,*,#2576,.T.);
#3616=ORIENTED_EDGE('',*,*,#2577,.F.);
#3617=ORIENTED_EDGE('',*,*,#2578,.F.);
#3618=ORIENTED_EDGE('',*,*,#2579,.F.);
#3619=ORIENTED_EDGE('',*,*,#2573,.T.);
#3620=ORIENTED_EDGE('',*,*,#2580,.T.);
#3621=ORIENTED_EDGE('',*,*,#2581,.T.);
#3622=ORIENTED_EDGE('',*,*,#2582,.F.);
#3623=ORIENTED_EDGE('',*,*,#2583,.F.);
#3624=ORIENTED_EDGE('',*,*,#2577,.T.);
#3625=ORIENTED_EDGE('',*,*,#2584,.T.);
#3626=ORIENTED_EDGE('',*,*,#2585,.F.);
#3627=ORIENTED_EDGE('',*,*,#2586,.F.);
#3628=ORIENTED_EDGE('',*,*,#2587,.F.);
#3629=ORIENTED_EDGE('',*,*,#2582,.T.);
#3630=ORIENTED_EDGE('',*,*,#2588,.T.);
#3631=ORIENTED_EDGE('',*,*,#2589,.T.);
#3632=ORIENTED_EDGE('',*,*,#2590,.T.);
#3633=ORIENTED_EDGE('',*,*,#2591,.F.);
#3634=ORIENTED_EDGE('',*,*,#2592,.T.);
#3635=ORIENTED_EDGE('',*,*,#2593,.T.);
#3636=ORIENTED_EDGE('',*,*,#2594,.T.);
#3637=ORIENTED_EDGE('',*,*,#2595,.T.);
#3638=ORIENTED_EDGE('',*,*,#2596,.T.);
#3639=ORIENTED_EDGE('',*,*,#2597,.T.);
#3640=ORIENTED_EDGE('',*,*,#2598,.T.);
#3641=ORIENTED_EDGE('',*,*,#2599,.T.);
#3642=ORIENTED_EDGE('',*,*,#2600,.T.);
#3643=ORIENTED_EDGE('',*,*,#2601,.T.);
#3644=ORIENTED_EDGE('',*,*,#2602,.T.);
#3645=ORIENTED_EDGE('',*,*,#2603,.T.);
#3646=ORIENTED_EDGE('',*,*,#2604,.T.);
#3647=ORIENTED_EDGE('',*,*,#2605,.T.);
#3648=ORIENTED_EDGE('',*,*,#2606,.T.);
#3649=ORIENTED_EDGE('',*,*,#2607,.T.);
#3650=ORIENTED_EDGE('',*,*,#2608,.T.);
#3651=ORIENTED_EDGE('',*,*,#2609,.T.);
#3652=ORIENTED_EDGE('',*,*,#2610,.T.);
#3653=ORIENTED_EDGE('',*,*,#2611,.T.);
#3654=ORIENTED_EDGE('',*,*,#2612,.T.);
#3655=ORIENTED_EDGE('',*,*,#2613,.T.);
#3656=ORIENTED_EDGE('',*,*,#2614,.T.);
#3657=ORIENTED_EDGE('',*,*,#2615,.T.);
#3658=ORIENTED_EDGE('',*,*,#2616,.T.);
#3659=ORIENTED_EDGE('',*,*,#2617,.T.);
#3660=ORIENTED_EDGE('',*,*,#2618,.T.);
#3661=ORIENTED_EDGE('',*,*,#2619,.T.);
#3662=ORIENTED_EDGE('',*,*,#2620,.T.);
#3663=ORIENTED_EDGE('',*,*,#2621,.T.);
#3664=ORIENTED_EDGE('',*,*,#2622,.T.);
#3665=ORIENTED_EDGE('',*,*,#2623,.T.);
#3666=ORIENTED_EDGE('',*,*,#2624,.T.);
#3667=ORIENTED_EDGE('',*,*,#2625,.T.);
#3668=ORIENTED_EDGE('',*,*,#2626,.T.);
#3669=ORIENTED_EDGE('',*,*,#2627,.T.);
#3670=ORIENTED_EDGE('',*,*,#2628,.T.);
#3671=ORIENTED_EDGE('',*,*,#2629,.T.);
#3672=ORIENTED_EDGE('',*,*,#2630,.T.);
#3673=ORIENTED_EDGE('',*,*,#2631,.T.);
#3674=ORIENTED_EDGE('',*,*,#2632,.T.);
#3675=ORIENTED_EDGE('',*,*,#2633,.T.);
#3676=ORIENTED_EDGE('',*,*,#2634,.T.);
#3677=ORIENTED_EDGE('',*,*,#2635,.T.);
#3678=ORIENTED_EDGE('',*,*,#2636,.T.);
#3679=ORIENTED_EDGE('',*,*,#2637,.T.);
#3680=ORIENTED_EDGE('',*,*,#2638,.T.);
#3681=ORIENTED_EDGE('',*,*,#2639,.T.);
#3682=ORIENTED_EDGE('',*,*,#2640,.T.);
#3683=ORIENTED_EDGE('',*,*,#2641,.T.);
#3684=ORIENTED_EDGE('',*,*,#2642,.T.);
#3685=ORIENTED_EDGE('',*,*,#2643,.T.);
#3686=ORIENTED_EDGE('',*,*,#2644,.T.);
#3687=ORIENTED_EDGE('',*,*,#2645,.T.);
#3688=ORIENTED_EDGE('',*,*,#2646,.T.);
#3689=ORIENTED_EDGE('',*,*,#2647,.T.);
#3690=ORIENTED_EDGE('',*,*,#2648,.T.);
#3691=ORIENTED_EDGE('',*,*,#2649,.T.);
#3692=ORIENTED_EDGE('',*,*,#2650,.T.);
#3693=ORIENTED_EDGE('',*,*,#2651,.T.);
#3694=ORIENTED_EDGE('',*,*,#2652,.T.);
#3695=ORIENTED_EDGE('',*,*,#2653,.T.);
#3696=ORIENTED_EDGE('',*,*,#2654,.T.);
#3697=ORIENTED_EDGE('',*,*,#2655,.T.);
#3698=ORIENTED_EDGE('',*,*,#2656,.T.);
#3699=ORIENTED_EDGE('',*,*,#2657,.T.);
#3700=ORIENTED_EDGE('',*,*,#2658,.T.);
#3701=ORIENTED_EDGE('',*,*,#2659,.T.);
#3702=ORIENTED_EDGE('',*,*,#2660,.T.);
#3703=ORIENTED_EDGE('',*,*,#2661,.T.);
#3704=ORIENTED_EDGE('',*,*,#2662,.T.);
#3705=ORIENTED_EDGE('',*,*,#2663,.T.);
#3706=ORIENTED_EDGE('',*,*,#2664,.T.);
#3707=ORIENTED_EDGE('',*,*,#2665,.T.);
#3708=ORIENTED_EDGE('',*,*,#2666,.T.);
#3709=ORIENTED_EDGE('',*,*,#2667,.T.);
#3710=ORIENTED_EDGE('',*,*,#2668,.T.);
#3711=ORIENTED_EDGE('',*,*,#2669,.T.);
#3712=ORIENTED_EDGE('',*,*,#2670,.T.);
#3713=ORIENTED_EDGE('',*,*,#2671,.T.);
#3714=ORIENTED_EDGE('',*,*,#2672,.T.);
#3715=ORIENTED_EDGE('',*,*,#2673,.T.);
#3716=ORIENTED_EDGE('',*,*,#2674,.T.);
#3717=ORIENTED_EDGE('',*,*,#2675,.T.);
#3718=ORIENTED_EDGE('',*,*,#2676,.T.);
#3719=ORIENTED_EDGE('',*,*,#2677,.F.);
#3720=ORIENTED_EDGE('',*,*,#2678,.T.);
#3721=ORIENTED_EDGE('',*,*,#2679,.T.);
#3722=ORIENTED_EDGE('',*,*,#2680,.T.);
#3723=ORIENTED_EDGE('',*,*,#2681,.T.);
#3724=ORIENTED_EDGE('',*,*,#2682,.T.);
#3725=ORIENTED_EDGE('',*,*,#2683,.T.);
#3726=ORIENTED_EDGE('',*,*,#2684,.T.);
#3727=ORIENTED_EDGE('',*,*,#2685,.T.);
#3728=ORIENTED_EDGE('',*,*,#2686,.T.);
#3729=ORIENTED_EDGE('',*,*,#2687,.T.);
#3730=ORIENTED_EDGE('',*,*,#2688,.T.);
#3731=ORIENTED_EDGE('',*,*,#2689,.T.);
#3732=ORIENTED_EDGE('',*,*,#2690,.T.);
#3733=ORIENTED_EDGE('',*,*,#2691,.T.);
#3734=ORIENTED_EDGE('',*,*,#2692,.T.);
#3735=ORIENTED_EDGE('',*,*,#2693,.T.);
#3736=ORIENTED_EDGE('',*,*,#2694,.T.);
#3737=ORIENTED_EDGE('',*,*,#2695,.T.);
#3738=ORIENTED_EDGE('',*,*,#2696,.T.);
#3739=ORIENTED_EDGE('',*,*,#2697,.T.);
#3740=ORIENTED_EDGE('',*,*,#2698,.T.);
#3741=ORIENTED_EDGE('',*,*,#2699,.T.);
#3742=ORIENTED_EDGE('',*,*,#2700,.T.);
#3743=ORIENTED_EDGE('',*,*,#2701,.T.);
#3744=ORIENTED_EDGE('',*,*,#2702,.T.);
#3745=ORIENTED_EDGE('',*,*,#2703,.T.);
#3746=ORIENTED_EDGE('',*,*,#2704,.T.);
#3747=ORIENTED_EDGE('',*,*,#2705,.T.);
#3748=ORIENTED_EDGE('',*,*,#2706,.T.);
#3749=ORIENTED_EDGE('',*,*,#2707,.T.);
#3750=ORIENTED_EDGE('',*,*,#2708,.T.);
#3751=ORIENTED_EDGE('',*,*,#2709,.T.);
#3752=ORIENTED_EDGE('',*,*,#2710,.T.);
#3753=ORIENTED_EDGE('',*,*,#2711,.T.);
#3754=ORIENTED_EDGE('',*,*,#2712,.T.);
#3755=ORIENTED_EDGE('',*,*,#2713,.T.);
#3756=ORIENTED_EDGE('',*,*,#2714,.T.);
#3757=ORIENTED_EDGE('',*,*,#2715,.T.);
#3758=ORIENTED_EDGE('',*,*,#2716,.T.);
#3759=ORIENTED_EDGE('',*,*,#2717,.T.);
#3760=ORIENTED_EDGE('',*,*,#2718,.T.);
#3761=ORIENTED_EDGE('',*,*,#2719,.T.);
#3762=ORIENTED_EDGE('',*,*,#2720,.T.);
#3763=ORIENTED_EDGE('',*,*,#2721,.T.);
#3764=ORIENTED_EDGE('',*,*,#2722,.T.);
#3765=ORIENTED_EDGE('',*,*,#2723,.T.);
#3766=ORIENTED_EDGE('',*,*,#2724,.T.);
#3767=ORIENTED_EDGE('',*,*,#2725,.T.);
#3768=ORIENTED_EDGE('',*,*,#2726,.T.);
#3769=ORIENTED_EDGE('',*,*,#2727,.T.);
#3770=ORIENTED_EDGE('',*,*,#2728,.T.);
#3771=ORIENTED_EDGE('',*,*,#2729,.T.);
#3772=ORIENTED_EDGE('',*,*,#2730,.T.);
#3773=ORIENTED_EDGE('',*,*,#2731,.T.);
#3774=ORIENTED_EDGE('',*,*,#2732,.T.);
#3775=ORIENTED_EDGE('',*,*,#2733,.T.);
#3776=ORIENTED_EDGE('',*,*,#2734,.T.);
#3777=ORIENTED_EDGE('',*,*,#2735,.T.);
#3778=ORIENTED_EDGE('',*,*,#2736,.T.);
#3779=ORIENTED_EDGE('',*,*,#2737,.T.);
#3780=ORIENTED_EDGE('',*,*,#2738,.T.);
#3781=ORIENTED_EDGE('',*,*,#2739,.T.);
#3782=ORIENTED_EDGE('',*,*,#2740,.T.);
#3783=ORIENTED_EDGE('',*,*,#2741,.T.);
#3784=ORIENTED_EDGE('',*,*,#2742,.T.);
#3785=ORIENTED_EDGE('',*,*,#2743,.T.);
#3786=ORIENTED_EDGE('',*,*,#2744,.T.);
#3787=ORIENTED_EDGE('',*,*,#2745,.T.);
#3788=ORIENTED_EDGE('',*,*,#2746,.T.);
#3789=ORIENTED_EDGE('',*,*,#2747,.T.);
#3790=ORIENTED_EDGE('',*,*,#2748,.T.);
#3791=ORIENTED_EDGE('',*,*,#2749,.T.);
#3792=ORIENTED_EDGE('',*,*,#2750,.T.);
#3793=ORIENTED_EDGE('',*,*,#2751,.T.);
#3794=ORIENTED_EDGE('',*,*,#2752,.T.);
#3795=ORIENTED_EDGE('',*,*,#2753,.T.);
#3796=ORIENTED_EDGE('',*,*,#2754,.T.);
#3797=ORIENTED_EDGE('',*,*,#2755,.T.);
#3798=ORIENTED_EDGE('',*,*,#2756,.T.);
#3799=ORIENTED_EDGE('',*,*,#2757,.T.);
#3800=ORIENTED_EDGE('',*,*,#2758,.T.);
#3801=ORIENTED_EDGE('',*,*,#2759,.T.);
#3802=ORIENTED_EDGE('',*,*,#2760,.T.);
#3803=ORIENTED_EDGE('',*,*,#2761,.T.);
#3804=ORIENTED_EDGE('',*,*,#2585,.T.);
#3805=ORIENTED_EDGE('',*,*,#2762,.T.);
#3806=ORIENTED_EDGE('',*,*,#2763,.F.);
#3807=ORIENTED_EDGE('',*,*,#2764,.F.);
#3808=ORIENTED_EDGE('',*,*,#2765,.F.);
#3809=ORIENTED_EDGE('',*,*,#2766,.F.);
#3810=ORIENTED_EDGE('',*,*,#2676,.F.);
#3811=ORIENTED_EDGE('',*,*,#2675,.F.);
#3812=ORIENTED_EDGE('',*,*,#2674,.F.);
#3813=ORIENTED_EDGE('',*,*,#2673,.F.);
#3814=ORIENTED_EDGE('',*,*,#2672,.F.);
#3815=ORIENTED_EDGE('',*,*,#2671,.F.);
#3816=ORIENTED_EDGE('',*,*,#2670,.F.);
#3817=ORIENTED_EDGE('',*,*,#2669,.F.);
#3818=ORIENTED_EDGE('',*,*,#2668,.F.);
#3819=ORIENTED_EDGE('',*,*,#2667,.F.);
#3820=ORIENTED_EDGE('',*,*,#2666,.F.);
#3821=ORIENTED_EDGE('',*,*,#2665,.F.);
#3822=ORIENTED_EDGE('',*,*,#2664,.F.);
#3823=ORIENTED_EDGE('',*,*,#2663,.F.);
#3824=ORIENTED_EDGE('',*,*,#2662,.F.);
#3825=ORIENTED_EDGE('',*,*,#2661,.F.);
#3826=ORIENTED_EDGE('',*,*,#2660,.F.);
#3827=ORIENTED_EDGE('',*,*,#2659,.F.);
#3828=ORIENTED_EDGE('',*,*,#2658,.F.);
#3829=ORIENTED_EDGE('',*,*,#2657,.F.);
#3830=ORIENTED_EDGE('',*,*,#2656,.F.);
#3831=ORIENTED_EDGE('',*,*,#2655,.F.);
#3832=ORIENTED_EDGE('',*,*,#2654,.F.);
#3833=ORIENTED_EDGE('',*,*,#2653,.F.);
#3834=ORIENTED_EDGE('',*,*,#2652,.F.);
#3835=ORIENTED_EDGE('',*,*,#2651,.F.);
#3836=ORIENTED_EDGE('',*,*,#2650,.F.);
#3837=ORIENTED_EDGE('',*,*,#2649,.F.);
#3838=ORIENTED_EDGE('',*,*,#2648,.F.);
#3839=ORIENTED_EDGE('',*,*,#2647,.F.);
#3840=ORIENTED_EDGE('',*,*,#2646,.F.);
#3841=ORIENTED_EDGE('',*,*,#2645,.F.);
#3842=ORIENTED_EDGE('',*,*,#2644,.F.);
#3843=ORIENTED_EDGE('',*,*,#2643,.F.);
#3844=ORIENTED_EDGE('',*,*,#2642,.F.);
#3845=ORIENTED_EDGE('',*,*,#2641,.F.);
#3846=ORIENTED_EDGE('',*,*,#2640,.F.);
#3847=ORIENTED_EDGE('',*,*,#2639,.F.);
#3848=ORIENTED_EDGE('',*,*,#2638,.F.);
#3849=ORIENTED_EDGE('',*,*,#2637,.F.);
#3850=ORIENTED_EDGE('',*,*,#2636,.F.);
#3851=ORIENTED_EDGE('',*,*,#2635,.F.);
#3852=ORIENTED_EDGE('',*,*,#2634,.F.);
#3853=ORIENTED_EDGE('',*,*,#2633,.F.);
#3854=ORIENTED_EDGE('',*,*,#2632,.F.);
#3855=ORIENTED_EDGE('',*,*,#2631,.F.);
#3856=ORIENTED_EDGE('',*,*,#2630,.F.);
#3857=ORIENTED_EDGE('',*,*,#2629,.F.);
#3858=ORIENTED_EDGE('',*,*,#2628,.F.);
#3859=ORIENTED_EDGE('',*,*,#2627,.F.);
#3860=ORIENTED_EDGE('',*,*,#2626,.F.);
#3861=ORIENTED_EDGE('',*,*,#2625,.F.);
#3862=ORIENTED_EDGE('',*,*,#2624,.F.);
#3863=ORIENTED_EDGE('',*,*,#2623,.F.);
#3864=ORIENTED_EDGE('',*,*,#2622,.F.);
#3865=ORIENTED_EDGE('',*,*,#2621,.F.);
#3866=ORIENTED_EDGE('',*,*,#2620,.F.);
#3867=ORIENTED_EDGE('',*,*,#2619,.F.);
#3868=ORIENTED_EDGE('',*,*,#2618,.F.);
#3869=ORIENTED_EDGE('',*,*,#2617,.F.);
#3870=ORIENTED_EDGE('',*,*,#2616,.F.);
#3871=ORIENTED_EDGE('',*,*,#2615,.F.);
#3872=ORIENTED_EDGE('',*,*,#2614,.F.);
#3873=ORIENTED_EDGE('',*,*,#2613,.F.);
#3874=ORIENTED_EDGE('',*,*,#2612,.F.);
#3875=ORIENTED_EDGE('',*,*,#2611,.F.);
#3876=ORIENTED_EDGE('',*,*,#2610,.F.);
#3877=ORIENTED_EDGE('',*,*,#2609,.F.);
#3878=ORIENTED_EDGE('',*,*,#2608,.F.);
#3879=ORIENTED_EDGE('',*,*,#2607,.F.);
#3880=ORIENTED_EDGE('',*,*,#2606,.F.);
#3881=ORIENTED_EDGE('',*,*,#2605,.F.);
#3882=ORIENTED_EDGE('',*,*,#2604,.F.);
#3883=ORIENTED_EDGE('',*,*,#2603,.F.);
#3884=ORIENTED_EDGE('',*,*,#2602,.F.);
#3885=ORIENTED_EDGE('',*,*,#2601,.F.);
#3886=ORIENTED_EDGE('',*,*,#2600,.F.);
#3887=ORIENTED_EDGE('',*,*,#2599,.F.);
#3888=ORIENTED_EDGE('',*,*,#2598,.F.);
#3889=ORIENTED_EDGE('',*,*,#2597,.F.);
#3890=ORIENTED_EDGE('',*,*,#2596,.F.);
#3891=ORIENTED_EDGE('',*,*,#2595,.F.);
#3892=ORIENTED_EDGE('',*,*,#2594,.F.);
#3893=ORIENTED_EDGE('',*,*,#2593,.F.);
#3894=ORIENTED_EDGE('',*,*,#2592,.F.);
#3895=ORIENTED_EDGE('',*,*,#2767,.F.);
#3896=ORIENTED_EDGE('',*,*,#2247,.T.);
#3897=ORIENTED_EDGE('',*,*,#2252,.T.);
#3898=ORIENTED_EDGE('',*,*,#2251,.T.);
#3899=ORIENTED_EDGE('',*,*,#2256,.T.);
#3900=ORIENTED_EDGE('',*,*,#2260,.T.);
#3901=ORIENTED_EDGE('',*,*,#2259,.T.);
#3902=ORIENTED_EDGE('',*,*,#2264,.T.);
#3903=ORIENTED_EDGE('',*,*,#2268,.T.);
#3904=ORIENTED_EDGE('',*,*,#2267,.T.);
#3905=ORIENTED_EDGE('',*,*,#2272,.T.);
#3906=ORIENTED_EDGE('',*,*,#2276,.T.);
#3907=ORIENTED_EDGE('',*,*,#2275,.T.);
#3908=ORIENTED_EDGE('',*,*,#2280,.T.);
#3909=ORIENTED_EDGE('',*,*,#2284,.T.);
#3910=ORIENTED_EDGE('',*,*,#2283,.T.);
#3911=ORIENTED_EDGE('',*,*,#2288,.T.);
#3912=ORIENTED_EDGE('',*,*,#2292,.T.);
#3913=ORIENTED_EDGE('',*,*,#2291,.T.);
#3914=ORIENTED_EDGE('',*,*,#2296,.T.);
#3915=ORIENTED_EDGE('',*,*,#2300,.T.);
#3916=ORIENTED_EDGE('',*,*,#2299,.T.);
#3917=ORIENTED_EDGE('',*,*,#2304,.T.);
#3918=ORIENTED_EDGE('',*,*,#2308,.T.);
#3919=ORIENTED_EDGE('',*,*,#2307,.T.);
#3920=ORIENTED_EDGE('',*,*,#2312,.T.);
#3921=ORIENTED_EDGE('',*,*,#2317,.T.);
#3922=ORIENTED_EDGE('',*,*,#2316,.T.);
#3923=ORIENTED_EDGE('',*,*,#2320,.T.);
#3924=ORIENTED_EDGE('',*,*,#2325,.T.);
#3925=ORIENTED_EDGE('',*,*,#2324,.T.);
#3926=ORIENTED_EDGE('',*,*,#2328,.T.);
#3927=ORIENTED_EDGE('',*,*,#2333,.T.);
#3928=ORIENTED_EDGE('',*,*,#2332,.T.);
#3929=ORIENTED_EDGE('',*,*,#2336,.T.);
#3930=ORIENTED_EDGE('',*,*,#2341,.T.);
#3931=ORIENTED_EDGE('',*,*,#2340,.T.);
#3932=ORIENTED_EDGE('',*,*,#2344,.T.);
#3933=ORIENTED_EDGE('',*,*,#2349,.T.);
#3934=ORIENTED_EDGE('',*,*,#2348,.T.);
#3935=ORIENTED_EDGE('',*,*,#2352,.T.);
#3936=ORIENTED_EDGE('',*,*,#2357,.T.);
#3937=ORIENTED_EDGE('',*,*,#2356,.T.);
#3938=ORIENTED_EDGE('',*,*,#2360,.T.);
#3939=ORIENTED_EDGE('',*,*,#2365,.T.);
#3940=ORIENTED_EDGE('',*,*,#2364,.T.);
#3941=ORIENTED_EDGE('',*,*,#2368,.T.);
#3942=ORIENTED_EDGE('',*,*,#2373,.T.);
#3943=ORIENTED_EDGE('',*,*,#2372,.T.);
#3944=ORIENTED_EDGE('',*,*,#2376,.T.);
#3945=ORIENTED_EDGE('',*,*,#2381,.T.);
#3946=ORIENTED_EDGE('',*,*,#2380,.T.);
#3947=ORIENTED_EDGE('',*,*,#2384,.T.);
#3948=ORIENTED_EDGE('',*,*,#2389,.T.);
#3949=ORIENTED_EDGE('',*,*,#2388,.T.);
#3950=ORIENTED_EDGE('',*,*,#2392,.T.);
#3951=ORIENTED_EDGE('',*,*,#2397,.T.);
#3952=ORIENTED_EDGE('',*,*,#2396,.T.);
#3953=ORIENTED_EDGE('',*,*,#2401,.T.);
#3954=ORIENTED_EDGE('',*,*,#2405,.T.);
#3955=ORIENTED_EDGE('',*,*,#2404,.T.);
#3956=ORIENTED_EDGE('',*,*,#2409,.T.);
#3957=ORIENTED_EDGE('',*,*,#2414,.T.);
#3958=ORIENTED_EDGE('',*,*,#2413,.T.);
#3959=ORIENTED_EDGE('',*,*,#2417,.T.);
#3960=ORIENTED_EDGE('',*,*,#2422,.T.);
#3961=ORIENTED_EDGE('',*,*,#2421,.T.);
#3962=ORIENTED_EDGE('',*,*,#2426,.T.);
#3963=ORIENTED_EDGE('',*,*,#2425,.T.);
#3964=ORIENTED_EDGE('',*,*,#2430,.T.);
#3965=ORIENTED_EDGE('',*,*,#2435,.T.);
#3966=ORIENTED_EDGE('',*,*,#2434,.T.);
#3967=ORIENTED_EDGE('',*,*,#2438,.T.);
#3968=ORIENTED_EDGE('',*,*,#2443,.T.);
#3969=ORIENTED_EDGE('',*,*,#2442,.T.);
#3970=ORIENTED_EDGE('',*,*,#2446,.T.);
#3971=ORIENTED_EDGE('',*,*,#2451,.T.);
#3972=ORIENTED_EDGE('',*,*,#2450,.T.);
#3973=ORIENTED_EDGE('',*,*,#2456,.T.);
#3974=ORIENTED_EDGE('',*,*,#2455,.T.);
#3975=ORIENTED_EDGE('',*,*,#2459,.T.);
#3976=ORIENTED_EDGE('',*,*,#2464,.T.);
#3977=ORIENTED_EDGE('',*,*,#2463,.T.);
#3978=ORIENTED_EDGE('',*,*,#2468,.T.);
#3979=ORIENTED_EDGE('',*,*,#2472,.T.);
#3980=ORIENTED_EDGE('',*,*,#2471,.T.);
#3981=ORIENTED_EDGE('',*,*,#2476,.T.);
#3982=ORIENTED_EDGE('',*,*,#2481,.T.);
#3983=ORIENTED_EDGE('',*,*,#2480,.T.);
#3984=ORIENTED_EDGE('',*,*,#2484,.T.);
#3985=ORIENTED_EDGE('',*,*,#2489,.T.);
#3986=ORIENTED_EDGE('',*,*,#2488,.T.);
#3987=ORIENTED_EDGE('',*,*,#2492,.T.);
#3988=ORIENTED_EDGE('',*,*,#2497,.T.);
#3989=ORIENTED_EDGE('',*,*,#2496,.T.);
#3990=ORIENTED_EDGE('',*,*,#2500,.T.);
#3991=ORIENTED_EDGE('',*,*,#2505,.T.);
#3992=ORIENTED_EDGE('',*,*,#2504,.T.);
#3993=ORIENTED_EDGE('',*,*,#2508,.T.);
#3994=ORIENTED_EDGE('',*,*,#2513,.T.);
#3995=ORIENTED_EDGE('',*,*,#2512,.T.);
#3996=ORIENTED_EDGE('',*,*,#2516,.T.);
#3997=ORIENTED_EDGE('',*,*,#2521,.T.);
#3998=ORIENTED_EDGE('',*,*,#2520,.T.);
#3999=ORIENTED_EDGE('',*,*,#2524,.T.);
#4000=ORIENTED_EDGE('',*,*,#2529,.T.);
#4001=ORIENTED_EDGE('',*,*,#2528,.T.);
#4002=ORIENTED_EDGE('',*,*,#2533,.T.);
#4003=ORIENTED_EDGE('',*,*,#2532,.T.);
#4004=ORIENTED_EDGE('',*,*,#2538,.T.);
#4005=ORIENTED_EDGE('',*,*,#2537,.T.);
#4006=ORIENTED_EDGE('',*,*,#2541,.T.);
#4007=ORIENTED_EDGE('',*,*,#2546,.T.);
#4008=ORIENTED_EDGE('',*,*,#2545,.T.);
#4009=ORIENTED_EDGE('',*,*,#2551,.T.);
#4010=ORIENTED_EDGE('',*,*,#2550,.T.);
#4011=ORIENTED_EDGE('',*,*,#2554,.T.);
#4012=ORIENTED_EDGE('',*,*,#2559,.T.);
#4013=ORIENTED_EDGE('',*,*,#2558,.T.);
#4014=ORIENTED_EDGE('',*,*,#2562,.T.);
#4015=ORIENTED_EDGE('',*,*,#2567,.T.);
#4016=ORIENTED_EDGE('',*,*,#2566,.T.);
#4017=ORIENTED_EDGE('',*,*,#2570,.T.);
#4018=ORIENTED_EDGE('',*,*,#2575,.T.);
#4019=ORIENTED_EDGE('',*,*,#2574,.T.);
#4020=ORIENTED_EDGE('',*,*,#2579,.T.);
#4021=ORIENTED_EDGE('',*,*,#2578,.T.);
#4022=ORIENTED_EDGE('',*,*,#2583,.T.);
#4023=ORIENTED_EDGE('',*,*,#2587,.T.);
#4024=ORIENTED_EDGE('',*,*,#2586,.T.);
#4025=ORIENTED_EDGE('',*,*,#2765,.T.);
#4026=ORIENTED_EDGE('',*,*,#2764,.T.);
#4027=ORIENTED_EDGE('',*,*,#2768,.F.);
#4028=ORIENTED_EDGE('',*,*,#2769,.F.);
#4029=ORIENTED_EDGE('',*,*,#2762,.F.);
#4030=ORIENTED_EDGE('',*,*,#2589,.F.);
#4031=ORIENTED_EDGE('',*,*,#2588,.F.);
#4032=ORIENTED_EDGE('',*,*,#2584,.F.);
#4033=ORIENTED_EDGE('',*,*,#2581,.F.);
#4034=ORIENTED_EDGE('',*,*,#2580,.F.);
#4035=ORIENTED_EDGE('',*,*,#2576,.F.);
#4036=ORIENTED_EDGE('',*,*,#2572,.F.);
#4037=ORIENTED_EDGE('',*,*,#2571,.F.);
#4038=ORIENTED_EDGE('',*,*,#2568,.F.);
#4039=ORIENTED_EDGE('',*,*,#2564,.F.);
#4040=ORIENTED_EDGE('',*,*,#2563,.F.);
#4041=ORIENTED_EDGE('',*,*,#2560,.F.);
#4042=ORIENTED_EDGE('',*,*,#2556,.F.);
#4043=ORIENTED_EDGE('',*,*,#2555,.F.);
#4044=ORIENTED_EDGE('',*,*,#2552,.F.);
#4045=ORIENTED_EDGE('',*,*,#2548,.F.);
#4046=ORIENTED_EDGE('',*,*,#2547,.F.);
#4047=ORIENTED_EDGE('',*,*,#2543,.F.);
#4048=ORIENTED_EDGE('',*,*,#2542,.F.);
#4049=ORIENTED_EDGE('',*,*,#2539,.F.);
#4050=ORIENTED_EDGE('',*,*,#2535,.F.);
#4051=ORIENTED_EDGE('',*,*,#2534,.F.);
#4052=ORIENTED_EDGE('',*,*,#2530,.F.);
#4053=ORIENTED_EDGE('',*,*,#2526,.F.);
#4054=ORIENTED_EDGE('',*,*,#2525,.F.);
#4055=ORIENTED_EDGE('',*,*,#2522,.F.);
#4056=ORIENTED_EDGE('',*,*,#2518,.F.);
#4057=ORIENTED_EDGE('',*,*,#2517,.F.);
#4058=ORIENTED_EDGE('',*,*,#2514,.F.);
#4059=ORIENTED_EDGE('',*,*,#2510,.F.);
#4060=ORIENTED_EDGE('',*,*,#2509,.F.);
#4061=ORIENTED_EDGE('',*,*,#2506,.F.);
#4062=ORIENTED_EDGE('',*,*,#2502,.F.);
#4063=ORIENTED_EDGE('',*,*,#2501,.F.);
#4064=ORIENTED_EDGE('',*,*,#2498,.F.);
#4065=ORIENTED_EDGE('',*,*,#2494,.F.);
#4066=ORIENTED_EDGE('',*,*,#2493,.F.);
#4067=ORIENTED_EDGE('',*,*,#2490,.F.);
#4068=ORIENTED_EDGE('',*,*,#2486,.F.);
#4069=ORIENTED_EDGE('',*,*,#2485,.F.);
#4070=ORIENTED_EDGE('',*,*,#2482,.F.);
#4071=ORIENTED_EDGE('',*,*,#2478,.F.);
#4072=ORIENTED_EDGE('',*,*,#2477,.F.);
#4073=ORIENTED_EDGE('',*,*,#2474,.F.);
#4074=ORIENTED_EDGE('',*,*,#2473,.F.);
#4075=ORIENTED_EDGE('',*,*,#2469,.F.);
#4076=ORIENTED_EDGE('',*,*,#2466,.F.);
#4077=ORIENTED_EDGE('',*,*,#2465,.F.);
#4078=ORIENTED_EDGE('',*,*,#2461,.F.);
#4079=ORIENTED_EDGE('',*,*,#2460,.F.);
#4080=ORIENTED_EDGE('',*,*,#2457,.F.);
#4081=ORIENTED_EDGE('',*,*,#2453,.F.);
#4082=ORIENTED_EDGE('',*,*,#2452,.F.);
#4083=ORIENTED_EDGE('',*,*,#2448,.F.);
#4084=ORIENTED_EDGE('',*,*,#2447,.F.);
#4085=ORIENTED_EDGE('',*,*,#2444,.F.);
#4086=ORIENTED_EDGE('',*,*,#2440,.F.);
#4087=ORIENTED_EDGE('',*,*,#2439,.F.);
#4088=ORIENTED_EDGE('',*,*,#2436,.F.);
#4089=ORIENTED_EDGE('',*,*,#2432,.F.);
#4090=ORIENTED_EDGE('',*,*,#2431,.F.);
#4091=ORIENTED_EDGE('',*,*,#2428,.F.);
#4092=ORIENTED_EDGE('',*,*,#2427,.F.);
#4093=ORIENTED_EDGE('',*,*,#2423,.F.);
#4094=ORIENTED_EDGE('',*,*,#2419,.F.);
#4095=ORIENTED_EDGE('',*,*,#2418,.F.);
#4096=ORIENTED_EDGE('',*,*,#2415,.F.);
#4097=ORIENTED_EDGE('',*,*,#2411,.F.);
#4098=ORIENTED_EDGE('',*,*,#2410,.F.);
#4099=ORIENTED_EDGE('',*,*,#2407,.F.);
#4100=ORIENTED_EDGE('',*,*,#2406,.F.);
#4101=ORIENTED_EDGE('',*,*,#2402,.F.);
#4102=ORIENTED_EDGE('',*,*,#2399,.F.);
#4103=ORIENTED_EDGE('',*,*,#2398,.F.);
#4104=ORIENTED_EDGE('',*,*,#2394,.F.);
#4105=ORIENTED_EDGE('',*,*,#2393,.F.);
#4106=ORIENTED_EDGE('',*,*,#2390,.F.);
#4107=ORIENTED_EDGE('',*,*,#2386,.F.);
#4108=ORIENTED_EDGE('',*,*,#2385,.F.);
#4109=ORIENTED_EDGE('',*,*,#2382,.F.);
#4110=ORIENTED_EDGE('',*,*,#2378,.F.);
#4111=ORIENTED_EDGE('',*,*,#2377,.F.);
#4112=ORIENTED_EDGE('',*,*,#2374,.F.);
#4113=ORIENTED_EDGE('',*,*,#2370,.F.);
#4114=ORIENTED_EDGE('',*,*,#2369,.F.);
#4115=ORIENTED_EDGE('',*,*,#2366,.F.);
#4116=ORIENTED_EDGE('',*,*,#2362,.F.);
#4117=ORIENTED_EDGE('',*,*,#2361,.F.);
#4118=ORIENTED_EDGE('',*,*,#2358,.F.);
#4119=ORIENTED_EDGE('',*,*,#2354,.F.);
#4120=ORIENTED_EDGE('',*,*,#2353,.F.);
#4121=ORIENTED_EDGE('',*,*,#2350,.F.);
#4122=ORIENTED_EDGE('',*,*,#2346,.F.);
#4123=ORIENTED_EDGE('',*,*,#2345,.F.);
#4124=ORIENTED_EDGE('',*,*,#2342,.F.);
#4125=ORIENTED_EDGE('',*,*,#2338,.F.);
#4126=ORIENTED_EDGE('',*,*,#2337,.F.);
#4127=ORIENTED_EDGE('',*,*,#2334,.F.);
#4128=ORIENTED_EDGE('',*,*,#2330,.F.);
#4129=ORIENTED_EDGE('',*,*,#2329,.F.);
#4130=ORIENTED_EDGE('',*,*,#2326,.F.);
#4131=ORIENTED_EDGE('',*,*,#2322,.F.);
#4132=ORIENTED_EDGE('',*,*,#2321,.F.);
#4133=ORIENTED_EDGE('',*,*,#2318,.F.);
#4134=ORIENTED_EDGE('',*,*,#2314,.F.);
#4135=ORIENTED_EDGE('',*,*,#2313,.F.);
#4136=ORIENTED_EDGE('',*,*,#2310,.F.);
#4137=ORIENTED_EDGE('',*,*,#2309,.F.);
#4138=ORIENTED_EDGE('',*,*,#2305,.F.);
#4139=ORIENTED_EDGE('',*,*,#2302,.F.);
#4140=ORIENTED_EDGE('',*,*,#2301,.F.);
#4141=ORIENTED_EDGE('',*,*,#2297,.F.);
#4142=ORIENTED_EDGE('',*,*,#2294,.F.);
#4143=ORIENTED_EDGE('',*,*,#2293,.F.);
#4144=ORIENTED_EDGE('',*,*,#2289,.F.);
#4145=ORIENTED_EDGE('',*,*,#2286,.F.);
#4146=ORIENTED_EDGE('',*,*,#2285,.F.);
#4147=ORIENTED_EDGE('',*,*,#2281,.F.);
#4148=ORIENTED_EDGE('',*,*,#2278,.F.);
#4149=ORIENTED_EDGE('',*,*,#2277,.F.);
#4150=ORIENTED_EDGE('',*,*,#2273,.F.);
#4151=ORIENTED_EDGE('',*,*,#2270,.F.);
#4152=ORIENTED_EDGE('',*,*,#2269,.F.);
#4153=ORIENTED_EDGE('',*,*,#2265,.F.);
#4154=ORIENTED_EDGE('',*,*,#2262,.F.);
#4155=ORIENTED_EDGE('',*,*,#2261,.F.);
#4156=ORIENTED_EDGE('',*,*,#2257,.F.);
#4157=ORIENTED_EDGE('',*,*,#2254,.F.);
#4158=ORIENTED_EDGE('',*,*,#2253,.F.);
#4159=ORIENTED_EDGE('',*,*,#2249,.F.);
#4160=ORIENTED_EDGE('',*,*,#2770,.F.);
#4161=ORIENTED_EDGE('',*,*,#2590,.F.);
#4162=ORIENTED_EDGE('',*,*,#2761,.F.);
#4163=ORIENTED_EDGE('',*,*,#2760,.F.);
#4164=ORIENTED_EDGE('',*,*,#2759,.F.);
#4165=ORIENTED_EDGE('',*,*,#2758,.F.);
#4166=ORIENTED_EDGE('',*,*,#2757,.F.);
#4167=ORIENTED_EDGE('',*,*,#2756,.F.);
#4168=ORIENTED_EDGE('',*,*,#2755,.F.);
#4169=ORIENTED_EDGE('',*,*,#2754,.F.);
#4170=ORIENTED_EDGE('',*,*,#2753,.F.);
#4171=ORIENTED_EDGE('',*,*,#2752,.F.);
#4172=ORIENTED_EDGE('',*,*,#2751,.F.);
#4173=ORIENTED_EDGE('',*,*,#2750,.F.);
#4174=ORIENTED_EDGE('',*,*,#2749,.F.);
#4175=ORIENTED_EDGE('',*,*,#2748,.F.);
#4176=ORIENTED_EDGE('',*,*,#2747,.F.);
#4177=ORIENTED_EDGE('',*,*,#2746,.F.);
#4178=ORIENTED_EDGE('',*,*,#2745,.F.);
#4179=ORIENTED_EDGE('',*,*,#2744,.F.);
#4180=ORIENTED_EDGE('',*,*,#2743,.F.);
#4181=ORIENTED_EDGE('',*,*,#2742,.F.);
#4182=ORIENTED_EDGE('',*,*,#2741,.F.);
#4183=ORIENTED_EDGE('',*,*,#2740,.F.);
#4184=ORIENTED_EDGE('',*,*,#2739,.F.);
#4185=ORIENTED_EDGE('',*,*,#2738,.F.);
#4186=ORIENTED_EDGE('',*,*,#2737,.F.);
#4187=ORIENTED_EDGE('',*,*,#2736,.F.);
#4188=ORIENTED_EDGE('',*,*,#2735,.F.);
#4189=ORIENTED_EDGE('',*,*,#2734,.F.);
#4190=ORIENTED_EDGE('',*,*,#2733,.F.);
#4191=ORIENTED_EDGE('',*,*,#2732,.F.);
#4192=ORIENTED_EDGE('',*,*,#2731,.F.);
#4193=ORIENTED_EDGE('',*,*,#2730,.F.);
#4194=ORIENTED_EDGE('',*,*,#2729,.F.);
#4195=ORIENTED_EDGE('',*,*,#2728,.F.);
#4196=ORIENTED_EDGE('',*,*,#2727,.F.);
#4197=ORIENTED_EDGE('',*,*,#2726,.F.);
#4198=ORIENTED_EDGE('',*,*,#2725,.F.);
#4199=ORIENTED_EDGE('',*,*,#2724,.F.);
#4200=ORIENTED_EDGE('',*,*,#2723,.F.);
#4201=ORIENTED_EDGE('',*,*,#2722,.F.);
#4202=ORIENTED_EDGE('',*,*,#2721,.F.);
#4203=ORIENTED_EDGE('',*,*,#2720,.F.);
#4204=ORIENTED_EDGE('',*,*,#2719,.F.);
#4205=ORIENTED_EDGE('',*,*,#2718,.F.);
#4206=ORIENTED_EDGE('',*,*,#2717,.F.);
#4207=ORIENTED_EDGE('',*,*,#2716,.F.);
#4208=ORIENTED_EDGE('',*,*,#2715,.F.);
#4209=ORIENTED_EDGE('',*,*,#2714,.F.);
#4210=ORIENTED_EDGE('',*,*,#2713,.F.);
#4211=ORIENTED_EDGE('',*,*,#2712,.F.);
#4212=ORIENTED_EDGE('',*,*,#2711,.F.);
#4213=ORIENTED_EDGE('',*,*,#2710,.F.);
#4214=ORIENTED_EDGE('',*,*,#2709,.F.);
#4215=ORIENTED_EDGE('',*,*,#2708,.F.);
#4216=ORIENTED_EDGE('',*,*,#2707,.F.);
#4217=ORIENTED_EDGE('',*,*,#2706,.F.);
#4218=ORIENTED_EDGE('',*,*,#2705,.F.);
#4219=ORIENTED_EDGE('',*,*,#2704,.F.);
#4220=ORIENTED_EDGE('',*,*,#2703,.F.);
#4221=ORIENTED_EDGE('',*,*,#2702,.F.);
#4222=ORIENTED_EDGE('',*,*,#2701,.F.);
#4223=ORIENTED_EDGE('',*,*,#2700,.F.);
#4224=ORIENTED_EDGE('',*,*,#2699,.F.);
#4225=ORIENTED_EDGE('',*,*,#2698,.F.);
#4226=ORIENTED_EDGE('',*,*,#2697,.F.);
#4227=ORIENTED_EDGE('',*,*,#2696,.F.);
#4228=ORIENTED_EDGE('',*,*,#2695,.F.);
#4229=ORIENTED_EDGE('',*,*,#2694,.F.);
#4230=ORIENTED_EDGE('',*,*,#2693,.F.);
#4231=ORIENTED_EDGE('',*,*,#2692,.F.);
#4232=ORIENTED_EDGE('',*,*,#2691,.F.);
#4233=ORIENTED_EDGE('',*,*,#2690,.F.);
#4234=ORIENTED_EDGE('',*,*,#2689,.F.);
#4235=ORIENTED_EDGE('',*,*,#2688,.F.);
#4236=ORIENTED_EDGE('',*,*,#2687,.F.);
#4237=ORIENTED_EDGE('',*,*,#2686,.F.);
#4238=ORIENTED_EDGE('',*,*,#2685,.F.);
#4239=ORIENTED_EDGE('',*,*,#2684,.F.);
#4240=ORIENTED_EDGE('',*,*,#2683,.F.);
#4241=ORIENTED_EDGE('',*,*,#2682,.F.);
#4242=ORIENTED_EDGE('',*,*,#2681,.F.);
#4243=ORIENTED_EDGE('',*,*,#2680,.F.);
#4244=ORIENTED_EDGE('',*,*,#2679,.F.);
#4245=ORIENTED_EDGE('',*,*,#2678,.F.);
#4246=ORIENTED_EDGE('',*,*,#2766,.T.);
#4247=ORIENTED_EDGE('',*,*,#2763,.T.);
#4248=ORIENTED_EDGE('',*,*,#2769,.T.);
#4249=ORIENTED_EDGE('',*,*,#2768,.T.);
#4250=ORIENTED_EDGE('',*,*,#2677,.T.);
#4251=ORIENTED_EDGE('',*,*,#2767,.T.);
#4252=ORIENTED_EDGE('',*,*,#2591,.T.);
#4253=ORIENTED_EDGE('',*,*,#2770,.T.);
#4254=ORIENTED_EDGE('',*,*,#2248,.T.);
#4301=CYLINDRICAL_SURFACE('',#4846,3.22275);
#4302=CYLINDRICAL_SURFACE('',#4848,3.22275);
#4303=CYLINDRICAL_SURFACE('',#4849,3.22275);
#4304=CYLINDRICAL_SURFACE('',#4850,3.22275);
#4305=CYLINDRICAL_SURFACE('',#4851,3.22275);
#4306=CYLINDRICAL_SURFACE('',#4852,3.22275);
#4307=CYLINDRICAL_SURFACE('',#4853,3.22275);
#4308=CYLINDRICAL_SURFACE('',#4854,3.22275);
#4309=CYLINDRICAL_SURFACE('',#4855,3.22275);
#4310=CYLINDRICAL_SURFACE('',#4856,3.22275);
#4311=CYLINDRICAL_SURFACE('',#4857,3.22275);
#4312=CYLINDRICAL_SURFACE('',#4858,3.22275);
#4313=CYLINDRICAL_SURFACE('',#4859,3.22275);
#4314=CYLINDRICAL_SURFACE('',#4860,3.22275);
#4315=CYLINDRICAL_SURFACE('',#4861,3.22275);
#4316=CYLINDRICAL_SURFACE('',#4862,3.22275);
#4317=CYLINDRICAL_SURFACE('',#4863,3.22275);
#4318=CYLINDRICAL_SURFACE('',#4864,3.22275);
#4319=CYLINDRICAL_SURFACE('',#4865,3.22275);
#4320=CYLINDRICAL_SURFACE('',#4866,3.22275);
#4321=CYLINDRICAL_SURFACE('',#4867,3.22275);
#4322=CYLINDRICAL_SURFACE('',#4868,3.22275);
#4323=CYLINDRICAL_SURFACE('',#4869,3.22275);
#4324=CYLINDRICAL_SURFACE('',#4870,3.22275);
#4325=CYLINDRICAL_SURFACE('',#4871,3.22275);
#4326=CYLINDRICAL_SURFACE('',#4872,3.22275);
#4327=CYLINDRICAL_SURFACE('',#4873,3.22275);
#4328=CYLINDRICAL_SURFACE('',#4874,3.22275);
#4329=CYLINDRICAL_SURFACE('',#4875,3.22275);
#4330=CYLINDRICAL_SURFACE('',#4876,3.22275);
#4331=CYLINDRICAL_SURFACE('',#4877,3.22275);
#4332=CYLINDRICAL_SURFACE('',#4878,3.22275);
#4333=CYLINDRICAL_SURFACE('',#4879,3.22275);
#4334=CYLINDRICAL_SURFACE('',#4880,3.22275);
#4335=CYLINDRICAL_SURFACE('',#4881,3.22275);
#4336=CYLINDRICAL_SURFACE('',#4882,3.22275);
#4337=CYLINDRICAL_SURFACE('',#4883,3.22275);
#4338=CYLINDRICAL_SURFACE('',#4884,3.22275);
#4339=CYLINDRICAL_SURFACE('',#4885,3.22275);
#4340=CYLINDRICAL_SURFACE('',#4886,3.22275);
#4341=CYLINDRICAL_SURFACE('',#4887,3.22275);
#4342=CYLINDRICAL_SURFACE('',#4888,3.22275);
#4343=CYLINDRICAL_SURFACE('',#4889,3.22275);
#4344=CYLINDRICAL_SURFACE('',#4890,3.22275);
#4345=CYLINDRICAL_SURFACE('',#4891,3.22275);
#4346=CYLINDRICAL_SURFACE('',#4892,3.22275);
#4347=CYLINDRICAL_SURFACE('',#4893,3.22275);
#4348=CYLINDRICAL_SURFACE('',#4894,3.22275);
#4349=CYLINDRICAL_SURFACE('',#4895,3.22275);
#4350=CYLINDRICAL_SURFACE('',#4896,3.22275);
#4351=CYLINDRICAL_SURFACE('',#4897,3.22275);
#4352=CYLINDRICAL_SURFACE('',#4898,3.22275);
#4353=CYLINDRICAL_SURFACE('',#4899,3.22275);
#4354=CYLINDRICAL_SURFACE('',#4900,3.22275);
#4355=CYLINDRICAL_SURFACE('',#4901,3.22275);
#4356=CYLINDRICAL_SURFACE('',#4902,3.22275);
#4357=CYLINDRICAL_SURFACE('',#4903,3.22275);
#4358=CYLINDRICAL_SURFACE('',#4904,3.22275);
#4359=CYLINDRICAL_SURFACE('',#4905,3.22275);
#4360=CYLINDRICAL_SURFACE('',#4906,3.22275);
#4361=CYLINDRICAL_SURFACE('',#4907,3.22275);
#4362=CYLINDRICAL_SURFACE('',#4908,3.22275);
#4363=CYLINDRICAL_SURFACE('',#4909,3.22275);
#4364=CYLINDRICAL_SURFACE('',#4910,3.22275);
#4365=CYLINDRICAL_SURFACE('',#4911,3.22275);
#4366=CYLINDRICAL_SURFACE('',#4912,3.22275);
#4367=CYLINDRICAL_SURFACE('',#4913,3.22275);
#4368=CYLINDRICAL_SURFACE('',#4914,3.22275);
#4369=CYLINDRICAL_SURFACE('',#4915,3.22275);
#4370=CYLINDRICAL_SURFACE('',#4916,3.22275);
#4371=CYLINDRICAL_SURFACE('',#4917,3.22275);
#4372=CYLINDRICAL_SURFACE('',#4918,3.22275);
#4373=CYLINDRICAL_SURFACE('',#4919,3.22275);
#4374=CYLINDRICAL_SURFACE('',#4920,3.22275);
#4375=CYLINDRICAL_SURFACE('',#4921,3.22275);
#4376=CYLINDRICAL_SURFACE('',#4922,3.22275);
#4377=CYLINDRICAL_SURFACE('',#4923,3.22275);
#4378=CYLINDRICAL_SURFACE('',#4924,3.22275);
#4379=CYLINDRICAL_SURFACE('',#4925,3.22275);
#4380=CYLINDRICAL_SURFACE('',#4926,3.22275);
#4381=CYLINDRICAL_SURFACE('',#4927,3.22275);
#4382=CYLINDRICAL_SURFACE('',#4928,3.22275);
#4383=CYLINDRICAL_SURFACE('',#4929,3.22275);
#4384=CYLINDRICAL_SURFACE('',#4930,3.22275);
#4385=CYLINDRICAL_SURFACE('',#4931,3.933);
#4386=CYLINDRICAL_SURFACE('',#4934,3.22275);
#4483=ADVANCED_FACE('',(#708),#4301,.T.);
#4484=ADVANCED_FACE('',(#709),#4302,.T.);
#4485=ADVANCED_FACE('',(#710),#4303,.T.);
#4486=ADVANCED_FACE('',(#711),#4304,.T.);
#4487=ADVANCED_FACE('',(#712),#4305,.T.);
#4488=ADVANCED_FACE('',(#713),#4306,.T.);
#4489=ADVANCED_FACE('',(#714),#4307,.T.);
#4490=ADVANCED_FACE('',(#715),#4308,.T.);
#4491=ADVANCED_FACE('',(#716),#4309,.T.);
#4492=ADVANCED_FACE('',(#717),#4310,.T.);
#4493=ADVANCED_FACE('',(#718),#4311,.T.);
#4494=ADVANCED_FACE('',(#719),#4312,.T.);
#4495=ADVANCED_FACE('',(#720),#4313,.T.);
#4496=ADVANCED_FACE('',(#721),#4314,.T.);
#4497=ADVANCED_FACE('',(#722),#4315,.T.);
#4498=ADVANCED_FACE('',(#723),#4316,.T.);
#4499=ADVANCED_FACE('',(#724),#4317,.T.);
#4500=ADVANCED_FACE('',(#725),#4318,.T.);
#4501=ADVANCED_FACE('',(#726),#4319,.T.);
#4502=ADVANCED_FACE('',(#727),#4320,.T.);
#4503=ADVANCED_FACE('',(#728),#4321,.T.);
#4504=ADVANCED_FACE('',(#729),#4322,.T.);
#4505=ADVANCED_FACE('',(#730),#4323,.T.);
#4506=ADVANCED_FACE('',(#731),#4324,.T.);
#4507=ADVANCED_FACE('',(#732),#4325,.T.);
#4508=ADVANCED_FACE('',(#733),#4326,.T.);
#4509=ADVANCED_FACE('',(#734),#4327,.T.);
#4510=ADVANCED_FACE('',(#735),#4328,.T.);
#4511=ADVANCED_FACE('',(#736),#4329,.T.);
#4512=ADVANCED_FACE('',(#737),#4330,.T.);
#4513=ADVANCED_FACE('',(#738),#4331,.T.);
#4514=ADVANCED_FACE('',(#739),#4332,.T.);
#4515=ADVANCED_FACE('',(#740),#4333,.T.);
#4516=ADVANCED_FACE('',(#741),#4334,.T.);
#4517=ADVANCED_FACE('',(#742),#4335,.T.);
#4518=ADVANCED_FACE('',(#743),#4336,.T.);
#4519=ADVANCED_FACE('',(#744),#4337,.T.);
#4520=ADVANCED_FACE('',(#745),#4338,.T.);
#4521=ADVANCED_FACE('',(#746),#4339,.T.);
#4522=ADVANCED_FACE('',(#747),#4340,.T.);
#4523=ADVANCED_FACE('',(#748),#4341,.T.);
#4524=ADVANCED_FACE('',(#749),#4342,.T.);
#4525=ADVANCED_FACE('',(#750),#4343,.T.);
#4526=ADVANCED_FACE('',(#751),#4344,.T.);
#4527=ADVANCED_FACE('',(#752),#4345,.T.);
#4528=ADVANCED_FACE('',(#753),#4346,.T.);
#4529=ADVANCED_FACE('',(#754),#4347,.T.);
#4530=ADVANCED_FACE('',(#755),#4348,.T.);
#4531=ADVANCED_FACE('',(#756),#4349,.T.);
#4532=ADVANCED_FACE('',(#757),#4350,.T.);
#4533=ADVANCED_FACE('',(#758),#4351,.T.);
#4534=ADVANCED_FACE('',(#759),#4352,.T.);
#4535=ADVANCED_FACE('',(#760),#4353,.T.);
#4536=ADVANCED_FACE('',(#761),#4354,.T.);
#4537=ADVANCED_FACE('',(#762),#4355,.T.);
#4538=ADVANCED_FACE('',(#763),#4356,.T.);
#4539=ADVANCED_FACE('',(#764),#4357,.T.);
#4540=ADVANCED_FACE('',(#765),#4358,.T.);
#4541=ADVANCED_FACE('',(#766),#4359,.T.);
#4542=ADVANCED_FACE('',(#767),#4360,.T.);
#4543=ADVANCED_FACE('',(#768),#4361,.T.);
#4544=ADVANCED_FACE('',(#769),#4362,.T.);
#4545=ADVANCED_FACE('',(#770),#4363,.T.);
#4546=ADVANCED_FACE('',(#771),#4364,.T.);
#4547=ADVANCED_FACE('',(#772),#4365,.T.);
#4548=ADVANCED_FACE('',(#773),#4366,.T.);
#4549=ADVANCED_FACE('',(#774),#4367,.T.);
#4550=ADVANCED_FACE('',(#775),#4368,.T.);
#4551=ADVANCED_FACE('',(#776),#4369,.T.);
#4552=ADVANCED_FACE('',(#777),#4370,.T.);
#4553=ADVANCED_FACE('',(#778),#4371,.T.);
#4554=ADVANCED_FACE('',(#779),#4372,.T.);
#4555=ADVANCED_FACE('',(#780),#4373,.T.);
#4556=ADVANCED_FACE('',(#781),#4374,.T.);
#4557=ADVANCED_FACE('',(#782),#4375,.T.);
#4558=ADVANCED_FACE('',(#783),#4376,.T.);
#4559=ADVANCED_FACE('',(#784),#4377,.T.);
#4560=ADVANCED_FACE('',(#785),#4378,.T.);
#4561=ADVANCED_FACE('',(#786),#4379,.T.);
#4562=ADVANCED_FACE('',(#787),#4380,.T.);
#4563=ADVANCED_FACE('',(#788),#4381,.T.);
#4564=ADVANCED_FACE('',(#789),#4382,.T.);
#4565=ADVANCED_FACE('',(#790),#4383,.T.);
#4566=ADVANCED_FACE('',(#791),#4384,.T.);
#4567=ADVANCED_FACE('',(#792),#4385,.T.);
#4568=ADVANCED_FACE('',(#793),#4386,.T.);
#4569=ADVANCED_FACE('',(#794),#47,.F.);
#4570=ADVANCED_FACE('',(#795),#48,.F.);
#4571=ADVANCED_FACE('',(#796),#610,.T.);
#4572=ADVANCED_FACE('',(#797),#611,.F.);
#4576=CLOSED_SHELL('',(#4483,#4484,#4485,#4486,#4487,#4488,#4489,#4490,
#4491,#4492,#4493,#4494,#4495,#4496,#4497,#4498,#4499,#4500,#4501,#4502,
#4503,#4504,#4505,#4506,#4507,#4508,#4509,#4510,#4511,#4512,#4513,#4514,
#4515,#4516,#4517,#4518,#4519,#4520,#4521,#4522,#4523,#4524,#4525,#4526,
#4527,#4528,#4529,#4530,#4531,#4532,#4533,#4534,#4535,#4536,#4537,#4538,
#4539,#4540,#4541,#4542,#4543,#4544,#4545,#4546,#4547,#4548,#4549,#4550,
#4551,#4552,#4553,#4554,#4555,#4556,#4557,#4558,#4559,#4560,#4561,#4562,
#4563,#4564,#4565,#4566,#4567,#4568,#4569,#4570,#4571,#4572));
#4845=AXIS2_PLACEMENT_3D('',#6223,#5487,#5488);
#4846=AXIS2_PLACEMENT_3D('',#6224,#5489,#5490);
#4847=AXIS2_PLACEMENT_3D('',#6342,#5492,#5493);
#4848=AXIS2_PLACEMENT_3D('',#6413,#5494,#5495);
#4849=AXIS2_PLACEMENT_3D('',#6986,#5497,#5498);
#4850=AXIS2_PLACEMENT_3D('',#7564,#5500,#5501);
#4851=AXIS2_PLACEMENT_3D('',#8156,#5503,#5504);
#4852=AXIS2_PLACEMENT_3D('',#8708,#5506,#5507);
#4853=AXIS2_PLACEMENT_3D('',#9316,#5509,#5510);
#4854=AXIS2_PLACEMENT_3D('',#9898,#5512,#5513);
#4855=AXIS2_PLACEMENT_3D('',#10514,#5515,#5516);
#4856=AXIS2_PLACEMENT_3D('',#11060,#5518,#5519);
#4857=AXIS2_PLACEMENT_3D('',#11694,#5521,#5522);
#4858=AXIS2_PLACEMENT_3D('',#12258,#5524,#5525);
#4859=AXIS2_PLACEMENT_3D('',#12872,#5527,#5528);
#4860=AXIS2_PLACEMENT_3D('',#13436,#5530,#5531);
#4861=AXIS2_PLACEMENT_3D('',#14044,#5533,#5534);
#4862=AXIS2_PLACEMENT_3D('',#14612,#5536,#5537);
#4863=AXIS2_PLACEMENT_3D('',#15204,#5539,#5540);
#4864=AXIS2_PLACEMENT_3D('',#15795,#5542,#5543);
#4865=AXIS2_PLACEMENT_3D('',#16426,#5545,#5546);
#4866=AXIS2_PLACEMENT_3D('',#17067,#5548,#5549);
#4867=AXIS2_PLACEMENT_3D('',#17610,#5551,#5552);
#4868=AXIS2_PLACEMENT_3D('',#18321,#5554,#5555);
#4869=AXIS2_PLACEMENT_3D('',#18926,#5557,#5558);
#4870=AXIS2_PLACEMENT_3D('',#19649,#5560,#5561);
#4871=AXIS2_PLACEMENT_3D('',#20216,#5563,#5564);
#4872=AXIS2_PLACEMENT_3D('',#20833,#5566,#5567);
#4873=AXIS2_PLACEMENT_3D('',#21420,#5569,#5570);
#4874=AXIS2_PLACEMENT_3D('',#22023,#5572,#5573);
#4875=AXIS2_PLACEMENT_3D('',#22616,#5575,#5576);
#4876=AXIS2_PLACEMENT_3D('',#23219,#5578,#5579);
#4877=AXIS2_PLACEMENT_3D('',#23824,#5581,#5582);
#4878=AXIS2_PLACEMENT_3D('',#24389,#5584,#5585);
#4879=AXIS2_PLACEMENT_3D('',#24964,#5587,#5588);
#4880=AXIS2_PLACEMENT_3D('',#25557,#5590,#5591);
#4881=AXIS2_PLACEMENT_3D('',#26108,#5593,#5594);
#4882=AXIS2_PLACEMENT_3D('',#26697,#5596,#5597);
#4883=AXIS2_PLACEMENT_3D('',#27308,#5599,#5600);
#4884=AXIS2_PLACEMENT_3D('',#27899,#5602,#5603);
#4885=AXIS2_PLACEMENT_3D('',#28485,#5605,#5606);
#4886=AXIS2_PLACEMENT_3D('',#29133,#5608,#5609);
#4887=AXIS2_PLACEMENT_3D('',#29641,#5611,#5612);
#4888=AXIS2_PLACEMENT_3D('',#30199,#5614,#5615);
#4889=AXIS2_PLACEMENT_3D('',#30810,#5617,#5618);
#4890=AXIS2_PLACEMENT_3D('',#31389,#5620,#5621);
#4891=AXIS2_PLACEMENT_3D('',#31942,#5623,#5624);
#4892=AXIS2_PLACEMENT_3D('',#32460,#5626,#5627);
#4893=AXIS2_PLACEMENT_3D('',#32987,#5629,#5630);
#4894=AXIS2_PLACEMENT_3D('',#33612,#5632,#5633);
#4895=AXIS2_PLACEMENT_3D('',#34193,#5635,#5636);
#4896=AXIS2_PLACEMENT_3D('',#34860,#5638,#5639);
#4897=AXIS2_PLACEMENT_3D('',#35393,#5641,#5642);
#4898=AXIS2_PLACEMENT_3D('',#35883,#5644,#5645);
#4899=AXIS2_PLACEMENT_3D('',#36442,#5647,#5648);
#4900=AXIS2_PLACEMENT_3D('',#37029,#5650,#5651);
#4901=AXIS2_PLACEMENT_3D('',#37619,#5653,#5654);
#4902=AXIS2_PLACEMENT_3D('',#38169,#5656,#5657);
#4903=AXIS2_PLACEMENT_3D('',#38697,#5659,#5660);
#4904=AXIS2_PLACEMENT_3D('',#39226,#5662,#5663);
#4905=AXIS2_PLACEMENT_3D('',#39813,#5665,#5666);
#4906=AXIS2_PLACEMENT_3D('',#40422,#5668,#5669);
#4907=AXIS2_PLACEMENT_3D('',#41059,#5671,#5672);
#4908=AXIS2_PLACEMENT_3D('',#41666,#5674,#5675);
#4909=AXIS2_PLACEMENT_3D('',#42259,#5677,#5678);
#4910=AXIS2_PLACEMENT_3D('',#42850,#5680,#5681);
#4911=AXIS2_PLACEMENT_3D('',#43453,#5683,#5684);
#4912=AXIS2_PLACEMENT_3D('',#44108,#5686,#5687);
#4913=AXIS2_PLACEMENT_3D('',#44753,#5689,#5690);
#4914=AXIS2_PLACEMENT_3D('',#45366,#5692,#5693);
#4915=AXIS2_PLACEMENT_3D('',#45949,#5695,#5696);
#4916=AXIS2_PLACEMENT_3D('',#46574,#5698,#5699);
#4917=AXIS2_PLACEMENT_3D('',#47129,#5701,#5702);
#4918=AXIS2_PLACEMENT_3D('',#47507,#5704,#5705);
#4919=AXIS2_PLACEMENT_3D('',#48014,#5707,#5708);
#4920=AXIS2_PLACEMENT_3D('',#48577,#5710,#5711);
#4921=AXIS2_PLACEMENT_3D('',#48938,#5713,#5714);
#4922=AXIS2_PLACEMENT_3D('',#49467,#5716,#5717);
#4923=AXIS2_PLACEMENT_3D('',#50060,#5719,#5720);
#4924=AXIS2_PLACEMENT_3D('',#50639,#5722,#5723);
#4925=AXIS2_PLACEMENT_3D('',#51208,#5725,#5726);
#4926=AXIS2_PLACEMENT_3D('',#51831,#5728,#5729);
#4927=AXIS2_PLACEMENT_3D('',#52430,#5731,#5732);
#4928=AXIS2_PLACEMENT_3D('',#52949,#5734,#5735);
#4929=AXIS2_PLACEMENT_3D('',#53535,#5737,#5738);
#4930=AXIS2_PLACEMENT_3D('',#54123,#5740,#5741);
#4931=AXIS2_PLACEMENT_3D('',#54675,#5743,#5744);
#4932=AXIS2_PLACEMENT_3D('',#54752,#5745,#5746);
#4933=AXIS2_PLACEMENT_3D('',#61716,#5747,#5748);
#4934=AXIS2_PLACEMENT_3D('',#69150,#5749,#5750);
#4935=AXIS2_PLACEMENT_3D('',#69327,#5751,#5752);
#4936=AXIS2_PLACEMENT_3D('',#74081,#5753,#5754);
#4937=AXIS2_PLACEMENT_3D('',#74082,#5755,#5756);
#5487=DIRECTION('axis',(0.,0.,1.));
#5488=DIRECTION('refdir',(1.,0.,0.));
#5489=DIRECTION('center_axis',(0.,0.,1.));
#5490=DIRECTION('ref_axis',(-0.45775083898785,-0.889080519079076,0.));
#5491=DIRECTION('',(0.,0.,-1.));
#5492=DIRECTION('center_axis',(0.,0.,-1.));
#5493=DIRECTION('ref_axis',(1.,-1.55574189099595E-12,0.));
#5494=DIRECTION('center_axis',(0.,0.,1.));
#5495=DIRECTION('ref_axis',(-0.45775083898785,-0.889080519079076,0.));
#5496=DIRECTION('',(0.,0.,-1.));
#5497=DIRECTION('center_axis',(0.,0.,1.));
#5498=DIRECTION('ref_axis',(-0.45775083898785,-0.889080519079076,0.));
#5499=DIRECTION('',(0.,0.,-1.));
#5500=DIRECTION('center_axis',(0.,0.,1.));
#5501=DIRECTION('ref_axis',(-0.45775083898785,-0.889080519079076,0.));
#5502=DIRECTION('',(0.,0.,-1.));
#5503=DIRECTION('center_axis',(0.,0.,1.));
#5504=DIRECTION('ref_axis',(-0.45775083898785,-0.889080519079076,0.));
#5505=DIRECTION('',(0.,0.,-1.));
#5506=DIRECTION('center_axis',(0.,0.,1.));
#5507=DIRECTION('ref_axis',(-0.45775083898785,-0.889080519079076,0.));
#5508=DIRECTION('',(0.,0.,-1.));
#5509=DIRECTION('center_axis',(0.,0.,1.));
#5510=DIRECTION('ref_axis',(-0.45775083898785,-0.889080519079076,0.));
#5511=DIRECTION('',(0.,0.,-1.));
#5512=DIRECTION('center_axis',(0.,0.,1.));
#5513=DIRECTION('ref_axis',(-0.45775083898785,-0.889080519079076,0.));
#5514=DIRECTION('',(0.,0.,-1.));
#5515=DIRECTION('center_axis',(0.,0.,1.));
#5516=DIRECTION('ref_axis',(-0.45775083898785,-0.889080519079076,0.));
#5517=DIRECTION('',(0.,0.,-1.));
#5518=DIRECTION('center_axis',(0.,0.,1.));
#5519=DIRECTION('ref_axis',(-0.45775083898785,-0.889080519079076,0.));
#5520=DIRECTION('',(0.,0.,-1.));
#5521=DIRECTION('center_axis',(0.,0.,1.));
#5522=DIRECTION('ref_axis',(-0.45775083898785,-0.889080519079076,0.));
#5523=DIRECTION('',(0.,0.,-1.));
#5524=DIRECTION('center_axis',(0.,0.,1.));
#5525=DIRECTION('ref_axis',(-0.45775083898785,-0.889080519079076,0.));
#5526=DIRECTION('',(0.,0.,-1.));
#5527=DIRECTION('center_axis',(0.,0.,1.));
#5528=DIRECTION('ref_axis',(-0.45775083898785,-0.889080519079076,0.));
#5529=DIRECTION('',(0.,0.,-1.));
#5530=DIRECTION('center_axis',(0.,0.,1.));
#5531=DIRECTION('ref_axis',(-0.45775083898785,-0.889080519079076,0.));
#5532=DIRECTION('',(0.,0.,-1.));
#5533=DIRECTION('center_axis',(0.,0.,1.));
#5534=DIRECTION('ref_axis',(-0.45775083898785,-0.889080519079076,0.));
#5535=DIRECTION('',(0.,0.,-1.));
#5536=DIRECTION('center_axis',(0.,0.,1.));
#5537=DIRECTION('ref_axis',(-0.45775083898785,-0.889080519079076,0.));
#5538=DIRECTION('',(0.,0.,-1.));
#5539=DIRECTION('center_axis',(0.,0.,1.));
#5540=DIRECTION('ref_axis',(-0.45775083898785,-0.889080519079076,0.));
#5541=DIRECTION('',(0.,0.,-1.));
#5542=DIRECTION('center_axis',(0.,0.,1.));
#5543=DIRECTION('ref_axis',(-0.45775083898785,-0.889080519079076,0.));
#5544=DIRECTION('',(0.,0.,-1.));
#5545=DIRECTION('center_axis',(0.,0.,1.));
#5546=DIRECTION('ref_axis',(-0.45775083898785,-0.889080519079076,0.));
#5547=DIRECTION('',(0.,0.,-1.));
#5548=DIRECTION('center_axis',(0.,0.,1.));
#5549=DIRECTION('ref_axis',(-0.45775083898785,-0.889080519079076,0.));
#5550=DIRECTION('',(0.,0.,-1.));
#5551=DIRECTION('center_axis',(0.,0.,1.));
#5552=DIRECTION('ref_axis',(-0.45775083898785,-0.889080519079076,0.));
#5553=DIRECTION('',(0.,0.,-1.));
#5554=DIRECTION('center_axis',(0.,0.,1.));
#5555=DIRECTION('ref_axis',(-0.45775083898785,-0.889080519079076,0.));
#5556=DIRECTION('',(0.,0.,-1.));
#5557=DIRECTION('center_axis',(0.,0.,1.));
#5558=DIRECTION('ref_axis',(-0.45775083898785,-0.889080519079076,0.));
#5559=DIRECTION('',(0.,0.,-1.));
#5560=DIRECTION('center_axis',(0.,0.,1.));
#5561=DIRECTION('ref_axis',(-0.45775083898785,-0.889080519079076,0.));
#5562=DIRECTION('',(0.,0.,-1.));
#5563=DIRECTION('center_axis',(0.,0.,1.));
#5564=DIRECTION('ref_axis',(-0.45775083898785,-0.889080519079076,0.));
#5565=DIRECTION('',(0.,0.,-1.));
#5566=DIRECTION('center_axis',(0.,0.,1.));
#5567=DIRECTION('ref_axis',(-0.45775083898785,-0.889080519079076,0.));
#5568=DIRECTION('',(0.,0.,-1.));
#5569=DIRECTION('center_axis',(0.,0.,1.));
#5570=DIRECTION('ref_axis',(-0.45775083898785,-0.889080519079076,0.));
#5571=DIRECTION('',(0.,0.,-1.));
#5572=DIRECTION('center_axis',(0.,0.,1.));
#5573=DIRECTION('ref_axis',(-0.45775083898785,-0.889080519079076,0.));
#5574=DIRECTION('',(0.,0.,-1.));
#5575=DIRECTION('center_axis',(0.,0.,1.));
#5576=DIRECTION('ref_axis',(-0.45775083898785,-0.889080519079076,0.));
#5577=DIRECTION('',(0.,0.,-1.));
#5578=DIRECTION('center_axis',(0.,0.,1.));
#5579=DIRECTION('ref_axis',(-0.45775083898785,-0.889080519079076,0.));
#5580=DIRECTION('',(0.,0.,-1.));
#5581=DIRECTION('center_axis',(0.,0.,1.));
#5582=DIRECTION('ref_axis',(-0.45775083898785,-0.889080519079076,0.));
#5583=DIRECTION('',(0.,0.,-1.));
#5584=DIRECTION('center_axis',(0.,0.,1.));
#5585=DIRECTION('ref_axis',(-0.45775083898785,-0.889080519079076,0.));
#5586=DIRECTION('',(0.,0.,-1.));
#5587=DIRECTION('center_axis',(0.,0.,1.));
#5588=DIRECTION('ref_axis',(-0.45775083898785,-0.889080519079076,0.));
#5589=DIRECTION('',(0.,0.,-1.));
#5590=DIRECTION('center_axis',(0.,0.,1.));
#5591=DIRECTION('ref_axis',(-0.45775083898785,-0.889080519079076,0.));
#5592=DIRECTION('',(0.,0.,-1.));
#5593=DIRECTION('center_axis',(0.,0.,1.));
#5594=DIRECTION('ref_axis',(-0.45775083898785,-0.889080519079076,0.));
#5595=DIRECTION('',(0.,0.,-1.));
#5596=DIRECTION('center_axis',(0.,0.,1.));
#5597=DIRECTION('ref_axis',(-0.45775083898785,-0.889080519079076,0.));
#5598=DIRECTION('',(0.,0.,-1.));
#5599=DIRECTION('center_axis',(0.,0.,1.));
#5600=DIRECTION('ref_axis',(-0.45775083898785,-0.889080519079076,0.));
#5601=DIRECTION('',(0.,0.,-1.));
#5602=DIRECTION('center_axis',(0.,0.,1.));
#5603=DIRECTION('ref_axis',(-0.45775083898785,-0.889080519079076,0.));
#5604=DIRECTION('',(0.,0.,-1.));
#5605=DIRECTION('center_axis',(0.,0.,1.));
#5606=DIRECTION('ref_axis',(-0.45775083898785,-0.889080519079076,0.));
#5607=DIRECTION('',(0.,0.,-1.));
#5608=DIRECTION('center_axis',(0.,0.,1.));
#5609=DIRECTION('ref_axis',(-0.45775083898785,-0.889080519079076,0.));
#5610=DIRECTION('',(0.,0.,-1.));
#5611=DIRECTION('center_axis',(0.,0.,1.));
#5612=DIRECTION('ref_axis',(-0.45775083898785,-0.889080519079076,0.));
#5613=DIRECTION('',(0.,0.,-1.));
#5614=DIRECTION('center_axis',(0.,0.,1.));
#5615=DIRECTION('ref_axis',(-0.45775083898785,-0.889080519079076,0.));
#5616=DIRECTION('',(0.,0.,-1.));
#5617=DIRECTION('center_axis',(0.,0.,1.));
#5618=DIRECTION('ref_axis',(-0.45775083898785,-0.889080519079076,0.));
#5619=DIRECTION('',(0.,0.,-1.));
#5620=DIRECTION('center_axis',(0.,0.,1.));
#5621=DIRECTION('ref_axis',(-0.45775083898785,-0.889080519079076,0.));
#5622=DIRECTION('',(0.,0.,-1.));
#5623=DIRECTION('center_axis',(0.,0.,1.));
#5624=DIRECTION('ref_axis',(-0.45775083898785,-0.889080519079076,0.));
#5625=DIRECTION('',(0.,0.,-1.));
#5626=DIRECTION('center_axis',(0.,0.,1.));
#5627=DIRECTION('ref_axis',(-0.45775083898785,-0.889080519079076,0.));
#5628=DIRECTION('',(0.,0.,-1.));
#5629=DIRECTION('center_axis',(0.,0.,1.));
#5630=DIRECTION('ref_axis',(-0.45775083898785,-0.889080519079076,0.));
#5631=DIRECTION('',(0.,0.,-1.));
#5632=DIRECTION('center_axis',(0.,0.,1.));
#5633=DIRECTION('ref_axis',(-0.45775083898785,-0.889080519079076,0.));
#5634=DIRECTION('',(0.,0.,-1.));
#5635=DIRECTION('center_axis',(0.,0.,1.));
#5636=DIRECTION('ref_axis',(-0.45775083898785,-0.889080519079076,0.));
#5637=DIRECTION('',(0.,0.,-1.));
#5638=DIRECTION('center_axis',(0.,0.,1.));
#5639=DIRECTION('ref_axis',(-0.45775083898785,-0.889080519079076,0.));
#5640=DIRECTION('',(0.,0.,-1.));
#5641=DIRECTION('center_axis',(0.,0.,1.));
#5642=DIRECTION('ref_axis',(-0.45775083898785,-0.889080519079076,0.));
#5643=DIRECTION('',(0.,0.,-1.));
#5644=DIRECTION('center_axis',(0.,0.,1.));
#5645=DIRECTION('ref_axis',(-0.45775083898785,-0.889080519079076,0.));
#5646=DIRECTION('',(0.,0.,-1.));
#5647=DIRECTION('center_axis',(0.,0.,1.));
#5648=DIRECTION('ref_axis',(-0.45775083898785,-0.889080519079076,0.));
#5649=DIRECTION('',(0.,0.,-1.));
#5650=DIRECTION('center_axis',(0.,0.,1.));
#5651=DIRECTION('ref_axis',(-0.45775083898785,-0.889080519079076,0.));
#5652=DIRECTION('',(0.,0.,-1.));
#5653=DIRECTION('center_axis',(0.,0.,1.));
#5654=DIRECTION('ref_axis',(-0.45775083898785,-0.889080519079076,0.));
#5655=DIRECTION('',(0.,0.,-1.));
#5656=DIRECTION('center_axis',(0.,0.,1.));
#5657=DIRECTION('ref_axis',(-0.45775083898785,-0.889080519079076,0.));
#5658=DIRECTION('',(0.,0.,-1.));
#5659=DIRECTION('center_axis',(0.,0.,1.));
#5660=DIRECTION('ref_axis',(-0.45775083898785,-0.889080519079076,0.));
#5661=DIRECTION('',(0.,0.,-1.));
#5662=DIRECTION('center_axis',(0.,0.,1.));
#5663=DIRECTION('ref_axis',(-0.45775083898785,-0.889080519079076,0.));
#5664=DIRECTION('',(0.,0.,-1.));
#5665=DIRECTION('center_axis',(0.,0.,1.));
#5666=DIRECTION('ref_axis',(-0.45775083898785,-0.889080519079076,0.));
#5667=DIRECTION('',(0.,0.,-1.));
#5668=DIRECTION('center_axis',(0.,0.,1.));
#5669=DIRECTION('ref_axis',(-0.45775083898785,-0.889080519079076,0.));
#5670=DIRECTION('',(0.,0.,-1.));
#5671=DIRECTION('center_axis',(0.,0.,1.));
#5672=DIRECTION('ref_axis',(-0.45775083898785,-0.889080519079076,0.));
#5673=DIRECTION('',(0.,0.,-1.));
#5674=DIRECTION('center_axis',(0.,0.,1.));
#5675=DIRECTION('ref_axis',(-0.45775083898785,-0.889080519079076,0.));
#5676=DIRECTION('',(0.,0.,-1.));
#5677=DIRECTION('center_axis',(0.,0.,1.));
#5678=DIRECTION('ref_axis',(-0.45775083898785,-0.889080519079076,0.));
#5679=DIRECTION('',(0.,0.,-1.));
#5680=DIRECTION('center_axis',(0.,0.,1.));
#5681=DIRECTION('ref_axis',(-0.45775083898785,-0.889080519079076,0.));
#5682=DIRECTION('',(0.,0.,-1.));
#5683=DIRECTION('center_axis',(0.,0.,1.));
#5684=DIRECTION('ref_axis',(-0.45775083898785,-0.889080519079076,0.));
#5685=DIRECTION('',(0.,0.,-1.));
#5686=DIRECTION('center_axis',(0.,0.,1.));
#5687=DIRECTION('ref_axis',(-0.45775083898785,-0.889080519079076,0.));
#5688=DIRECTION('',(0.,0.,-1.));
#5689=DIRECTION('center_axis',(0.,0.,1.));
#5690=DIRECTION('ref_axis',(-0.45775083898785,-0.889080519079076,0.));
#5691=DIRECTION('',(0.,0.,-1.));
#5692=DIRECTION('center_axis',(0.,0.,1.));
#5693=DIRECTION('ref_axis',(-0.45775083898785,-0.889080519079076,0.));
#5694=DIRECTION('',(0.,0.,-1.));
#5695=DIRECTION('center_axis',(0.,0.,1.));
#5696=DIRECTION('ref_axis',(-0.45775083898785,-0.889080519079076,0.));
#5697=DIRECTION('',(0.,0.,-1.));
#5698=DIRECTION('center_axis',(0.,0.,1.));
#5699=DIRECTION('ref_axis',(-0.45775083898785,-0.889080519079076,0.));
#5700=DIRECTION('',(0.,0.,-1.));
#5701=DIRECTION('center_axis',(0.,0.,1.));
#5702=DIRECTION('ref_axis',(-0.45775083898785,-0.889080519079076,0.));
#5703=DIRECTION('',(0.,0.,-1.));
#5704=DIRECTION('center_axis',(0.,0.,1.));
#5705=DIRECTION('ref_axis',(-0.45775083898785,-0.889080519079076,0.));
#5706=DIRECTION('',(0.,0.,-1.));
#5707=DIRECTION('center_axis',(0.,0.,1.));
#5708=DIRECTION('ref_axis',(-0.45775083898785,-0.889080519079076,0.));
#5709=DIRECTION('',(0.,0.,-1.));
#5710=DIRECTION('center_axis',(0.,0.,1.));
#5711=DIRECTION('ref_axis',(-0.45775083898785,-0.889080519079076,0.));
#5712=DIRECTION('',(0.,0.,-1.));
#5713=DIRECTION('center_axis',(0.,0.,1.));
#5714=DIRECTION('ref_axis',(-0.45775083898785,-0.889080519079076,0.));
#5715=DIRECTION('',(0.,0.,-1.));
#5716=DIRECTION('center_axis',(0.,0.,1.));
#5717=DIRECTION('ref_axis',(-0.45775083898785,-0.889080519079076,0.));
#5718=DIRECTION('',(0.,0.,-1.));
#5719=DIRECTION('center_axis',(0.,0.,1.));
#5720=DIRECTION('ref_axis',(-0.45775083898785,-0.889080519079076,0.));
#5721=DIRECTION('',(0.,0.,-1.));
#5722=DIRECTION('center_axis',(0.,0.,1.));
#5723=DIRECTION('ref_axis',(-0.45775083898785,-0.889080519079076,0.));
#5724=DIRECTION('',(0.,0.,-1.));
#5725=DIRECTION('center_axis',(0.,0.,1.));
#5726=DIRECTION('ref_axis',(-0.45775083898785,-0.889080519079076,0.));
#5727=DIRECTION('',(0.,0.,-1.));
#5728=DIRECTION('center_axis',(0.,0.,1.));
#5729=DIRECTION('ref_axis',(-0.45775083898785,-0.889080519079076,0.));
#5730=DIRECTION('',(0.,0.,-1.));
#5731=DIRECTION('center_axis',(0.,0.,1.));
#5732=DIRECTION('ref_axis',(-0.45775083898785,-0.889080519079076,0.));
#5733=DIRECTION('',(0.,0.,-1.));
#5734=DIRECTION('center_axis',(0.,0.,1.));
#5735=DIRECTION('ref_axis',(-0.45775083898785,-0.889080519079076,0.));
#5736=DIRECTION('',(0.,0.,-1.));
#5737=DIRECTION('center_axis',(0.,0.,1.));
#5738=DIRECTION('ref_axis',(-0.45775083898785,-0.889080519079076,0.));
#5739=DIRECTION('',(0.,0.,-1.));
#5740=DIRECTION('center_axis',(0.,0.,1.));
#5741=DIRECTION('ref_axis',(-0.45775083898785,-0.889080519079076,0.));
#5742=DIRECTION('',(0.,0.,-1.));
#5743=DIRECTION('center_axis',(0.,0.,1.));
#5744=DIRECTION('ref_axis',(1.,0.,0.));
#5745=DIRECTION('center_axis',(0.,0.,-1.));
#5746=DIRECTION('ref_axis',(1.,0.,0.));
#5747=DIRECTION('center_axis',(0.,0.,-1.));
#5748=DIRECTION('ref_axis',(1.,0.,0.));
#5749=DIRECTION('center_axis',(0.,0.,1.));
#5750=DIRECTION('ref_axis',(-0.45775083898785,-0.889080519079076,0.));
#5751=DIRECTION('center_axis',(0.,0.,1.));
#5752=DIRECTION('ref_axis',(1.,-1.55574189099595E-12,0.));
#5753=DIRECTION('center_axis',(0.,0.,1.));
#5754=DIRECTION('ref_axis',(1.,0.,0.));
#5755=DIRECTION('center_axis',(0.,0.,1.));
#5756=DIRECTION('ref_axis',(1.,0.,0.));
#6223=CARTESIAN_POINT('',(0.,0.,0.));
#6224=CARTESIAN_POINT('Origin',(-23.5502525316942,23.5502525316942,-77.3107734492734));
#6225=CARTESIAN_POINT('',(-22.0750360153461,26.4155367745563,-74.34623438385));
#6226=CARTESIAN_POINT('',(-22.0750360153461,26.4155367745563,-74.5928284611549));
#6227=CARTESIAN_POINT('',(-22.0750360153461,26.4155367745563,-77.3107734492734));
#6228=CARTESIAN_POINT('',(-25.4217763663954,20.9266069575655,-74.9999352075484));
#6229=CARTESIAN_POINT('Ctrl Pts',(-25.4217763663954,20.9266069575655,-74.9999352075484));
#6230=CARTESIAN_POINT('Ctrl Pts',(-25.3415113023851,20.8693515180845,-74.9938139384461));
#6231=CARTESIAN_POINT('Ctrl Pts',(-25.258468139995,20.8156772001763,-74.9876926693437));
#6232=CARTESIAN_POINT('Ctrl Pts',(-25.1730031022917,20.7658678333945,-74.9815714002414));
#6233=CARTESIAN_POINT('Ctrl Pts',(-25.087650312619,20.7161238852152,-74.9754581706886));
#6234=CARTESIAN_POINT('Ctrl Pts',(-24.9998823463237,20.6702350229595,-74.9693449411357));
#6235=CARTESIAN_POINT('Ctrl Pts',(-24.910086288991,20.6284432095419,-74.9632317115829));
#6236=CARTESIAN_POINT('Ctrl Pts',(-24.8183856393031,20.5857649833941,-74.9569888192073));
#6237=CARTESIAN_POINT('Ctrl Pts',(-24.7245702542372,20.5473598737791,-74.9507459268316));
#6238=CARTESIAN_POINT('Ctrl Pts',(-24.629081335484,20.5134374279031,-74.944503034456));
#6239=CARTESIAN_POINT('Ctrl Pts',(-24.5357311202979,20.4802747566371,-74.9383999666418));
#6240=CARTESIAN_POINT('Ctrl Pts',(-24.4407819924413,20.4513962064306,-74.9322968988277));
#6241=CARTESIAN_POINT('Ctrl Pts',(-24.3446673004952,20.4269493543496,-74.9261938310135));
#6242=CARTESIAN_POINT('Ctrl Pts',(-24.248581729055,20.4025099090935,-74.9200926122863));
#6243=CARTESIAN_POINT('Ctrl Pts',(-24.1513317232489,20.3824996035349,-74.9139913935591));
#6244=CARTESIAN_POINT('Ctrl Pts',(-24.0533648896118,20.3670158898765,-74.9078901748319));
#6245=CARTESIAN_POINT('Ctrl Pts',(-23.9554004768615,20.3515325588407,-74.9017891068737));
#6246=CARTESIAN_POINT('Ctrl Pts',(-23.8567197084106,20.34057566546,-74.8956880389155));
#6247=CARTESIAN_POINT('Ctrl Pts',(-23.7577783523882,20.3341911833606,-74.8895869709572));
#6248=CARTESIAN_POINT('Ctrl Pts',(-23.654820760349,20.3275475418157,-74.8832382479248));
#6249=CARTESIAN_POINT('Ctrl Pts',(-23.5515814925213,20.3258554514295,-74.8768895248922));
#6250=CARTESIAN_POINT('Ctrl Pts',(-23.4485758461978,20.3291068637483,-74.8705408018598));
#6251=CARTESIAN_POINT('Ctrl Pts',(-23.3494534047172,20.3322357012326,-74.8644314190276));
#6252=CARTESIAN_POINT('Ctrl Pts',(-23.2505477343847,20.3399419342038,-74.8583220361954));
#6253=CARTESIAN_POINT('Ctrl Pts',(-23.1523126956406,20.3521653769435,-74.8522126533633));
#6254=CARTESIAN_POINT('Ctrl Pts',(-23.0540112475345,20.3643970830385,-74.8460991404343));
#6255=CARTESIAN_POINT('Ctrl Pts',(-22.9563817675357,20.3811519995275,-74.8399856275054));
#6256=CARTESIAN_POINT('Ctrl Pts',(-22.8598671888174,20.4023189808007,-74.8338721145765));
#6257=CARTESIAN_POINT('Ctrl Pts',(-22.7632121778204,20.4235167608139,-74.8277497062603));
#6258=CARTESIAN_POINT('Ctrl Pts',(-22.6676757279364,20.4491392935652,-74.8216272979441));
#6259=CARTESIAN_POINT('Ctrl Pts',(-22.5736844908171,20.479025997549,-74.8155048896279));
#6260=CARTESIAN_POINT('Ctrl Pts',(-22.5629248082052,20.4824472893528,-74.8148040246077));
#6261=CARTESIAN_POINT('Ctrl Pts',(-22.5521853514869,20.4859244104502,-74.8141031595875));
#6262=CARTESIAN_POINT('Ctrl Pts',(-22.5414667417776,20.4894570807432,-74.8134022945673));
#6263=CARTESIAN_POINT('Ctrl Pts',(-22.4469052689154,20.5206229236182,-74.8072191392529));
#6264=CARTESIAN_POINT('Ctrl Pts',(-22.3536296772483,20.5562276387414,-74.8010359839384));
#6265=CARTESIAN_POINT('Ctrl Pts',(-22.2620859036837,20.5961461861169,-74.794852828624));
#6266=CARTESIAN_POINT('Ctrl Pts',(-22.1706627851161,20.6360121207146,-74.7886778227287));
#6267=CARTESIAN_POINT('Ctrl Pts',(-22.0809673405844,20.6801804139711,-74.7825028168334));
#6268=CARTESIAN_POINT('Ctrl Pts',(-21.9934295894148,20.7284765149111,-74.7763278109382));
#6269=CARTESIAN_POINT('Ctrl Pts',(-21.9059816187024,20.7767230824101,-74.7701591382517));
#6270=CARTESIAN_POINT('Ctrl Pts',(-21.820687318068,20.8290888320475,-74.7639904655652));
#6271=CARTESIAN_POINT('Ctrl Pts',(-21.7379551100751,20.8853518547284,-74.7578217928787));
#6272=CARTESIAN_POINT('Ctrl Pts',(-21.6552799289935,20.9415760955795,-74.7516573722285));
#6273=CARTESIAN_POINT('Ctrl Pts',(-21.5751636860409,21.0016920258799,-74.7454929515783));
#6274=CARTESIAN_POINT('Ctrl Pts',(-21.4979878736985,21.0654331547491,-74.7393285309281));
#6275=CARTESIAN_POINT('Ctrl Pts',(-21.4208394097242,21.129151696025,-74.7331662947297));
#6276=CARTESIAN_POINT('Ctrl Pts',(-21.3466296389297,21.196492607828,-74.7270040585313));
#6277=CARTESIAN_POINT('Ctrl Pts',(-21.2757081471388,21.2671481965427,-74.720841822333));
#6278=CARTESIAN_POINT('Ctrl Pts',(-21.2047930105908,21.337797453842,-74.7146801383298));
#6279=CARTESIAN_POINT('Ctrl Pts',(-21.1371658735867,21.4117604921122,-74.7085184543267));
#6280=CARTESIAN_POINT('Ctrl Pts',(-21.073139799602,21.4886924246377,-74.7023567703235));
#6281=CARTESIAN_POINT('Ctrl Pts',(-21.0091025120195,21.5656378311075,-74.6961940071561));
#6282=CARTESIAN_POINT('Ctrl Pts',(-20.9486678171902,21.6455528323533,-74.6900312439888));
#6283=CARTESIAN_POINT('Ctrl Pts',(-20.8921081564378,21.728059884691,-74.6838684808214));
#6284=CARTESIAN_POINT('Ctrl Pts',(-20.8354870738039,21.8106565369009,-74.6776990251014));
#6285=CARTESIAN_POINT('Ctrl Pts',(-20.7827496734932,21.895850503713,-74.6715295693814));
#6286=CARTESIAN_POINT('Ctrl Pts',(-20.7341246787443,21.9832357869402,-74.6653601136613));
#6287=CARTESIAN_POINT('Ctrl Pts',(-20.6854719686393,22.0706708781775,-74.6591871414646));
#6288=CARTESIAN_POINT('Ctrl Pts',(-20.640936524947,22.1602993860099,-74.6530141692678));
#6289=CARTESIAN_POINT('Ctrl Pts',(-20.6006998362459,22.2516931532777,-74.6468411970711));
#6290=CARTESIAN_POINT('Ctrl Pts',(-20.5603959140281,22.3432396350101,-74.6406579101432));
#6291=CARTESIAN_POINT('Ctrl Pts',(-20.5244052504831,22.4365568643179,-74.6344746232152));
#6292=CARTESIAN_POINT('Ctrl Pts',(-20.4928602248663,22.5311991255129,-74.6282913362873));
#6293=CARTESIAN_POINT('Ctrl Pts',(-20.4694334833756,22.6014846853995,-74.6236993519223));
#6294=CARTESIAN_POINT('Ctrl Pts',(-20.448457569277,22.6725006748828,-74.6191073675574));
#6295=CARTESIAN_POINT('Ctrl Pts',(-20.4299684107723,22.7440611355466,-74.6145153831924));
#6296=CARTESIAN_POINT('Ctrl Pts',(-20.4051527281407,22.8401077825774,-74.6083521374925));
#6297=CARTESIAN_POINT('Ctrl Pts',(-20.3847309724908,22.9374751239296,-74.6021888917926));
#6298=CARTESIAN_POINT('Ctrl Pts',(-20.3688412132802,23.0357240236724,-74.5960256460927));
#6299=CARTESIAN_POINT('Ctrl Pts',(-20.3529733103834,23.1338377823624,-74.5898708779178));
#6300=CARTESIAN_POINT('Ctrl Pts',(-20.3416250837045,23.2328302632332,-74.583716109743));
#6301=CARTESIAN_POINT('Ctrl Pts',(-20.3348844607828,23.3322485614009,-74.5775613415682));
#6302=CARTESIAN_POINT('Ctrl Pts',(-20.328151101818,23.4315597225525,-74.5714132060103));
#6303=CARTESIAN_POINT('Ctrl Pts',(-20.3260155052307,23.5312953564624,-74.5652650704526));
#6304=CARTESIAN_POINT('Ctrl Pts',(-20.3285141415369,23.6309947628186,-74.5591169348947));
#6305=CARTESIAN_POINT('Ctrl Pts',(-20.33101090078,23.7306192714827,-74.5529734180321));
#6306=CARTESIAN_POINT('Ctrl Pts',(-20.3381349607413,23.8302071723837,-74.5468299011694));
#6307=CARTESIAN_POINT('Ctrl Pts',(-20.3498707423274,23.9292960183673,-74.5406863843068));
#6308=CARTESIAN_POINT('Ctrl Pts',(-20.3616019334391,24.0283461055516,-74.534545270493));
#6309=CARTESIAN_POINT('Ctrl Pts',(-20.3779412109984,24.126897093364,-74.5284041566791));
#6310=CARTESIAN_POINT('Ctrl Pts',(-20.3988210640403,24.2244908183412,-74.5222630428653));
#6311=CARTESIAN_POINT('Ctrl Pts',(-20.4196983797654,24.3220726837427,-74.5161226753188));
#6312=CARTESIAN_POINT('Ctrl Pts',(-20.4451150829239,24.4186970913747,-74.5099823077723));
#6313=CARTESIAN_POINT('Ctrl Pts',(-20.4749525820067,24.513916260363,-74.5038419402258));
#6314=CARTESIAN_POINT('Ctrl Pts',(-20.5047945003841,24.6091495324626,-74.4977006632165));
#6315=CARTESIAN_POINT('Ctrl Pts',(-20.5390583847173,24.7029767366334,-74.4915593862072));
#6316=CARTESIAN_POINT('Ctrl Pts',(-20.5775761475754,24.7949664256483,-74.4854181091979));
#6317=CARTESIAN_POINT('Ctrl Pts',(-20.6161350597049,24.8870543890281,-74.4792702713436));
#6318=CARTESIAN_POINT('Ctrl Pts',(-20.6589567566051,24.9773005144231,-74.4731224334892));
#6319=CARTESIAN_POINT('Ctrl Pts',(-20.7058255140535,25.0652946115769,-74.4669745956349));
#6320=CARTESIAN_POINT('Ctrl Pts',(-20.7527202648339,25.1533375101054,-74.4608233482003));
#6321=CARTESIAN_POINT('Ctrl Pts',(-20.8036663231178,25.2391255185451,-74.4546721007656));
#6322=CARTESIAN_POINT('Ctrl Pts',(-20.8584037256175,25.3222761115947,-74.448520853331));
#6323=CARTESIAN_POINT('Ctrl Pts',(-20.9132333607873,25.4055668136167,-74.4423592410279));
#6324=CARTESIAN_POINT('Ctrl Pts',(-20.9718668443349,25.4862108707842,-74.4361976287249));
#6325=CARTESIAN_POINT('Ctrl Pts',(-21.0340028298801,25.5638575080042,-74.4300360164218));
#6326=CARTESIAN_POINT('Ctrl Pts',(-21.0824331724179,25.624377240724,-74.4252335015537));
#6327=CARTESIAN_POINT('Ctrl Pts',(-21.1329904450727,25.6830766640724,-74.4204309866857));
#6328=CARTESIAN_POINT('Ctrl Pts',(-21.1855169164876,25.7398056899147,-74.4156284718176));
#6329=CARTESIAN_POINT('Ctrl Pts',(-21.2530294424229,25.8127197792358,-74.4094557763966));
#6330=CARTESIAN_POINT('Ctrl Pts',(-21.3240358231561,25.8826362572171,-74.4032830809755));
#6331=CARTESIAN_POINT('Ctrl Pts',(-21.3982393509863,25.9492016417337,-74.3971103855545));
#6332=CARTESIAN_POINT('Ctrl Pts',(-21.4723549916283,26.0156881857337,-74.390945001118));
#6333=CARTESIAN_POINT('Ctrl Pts',(-21.5496599390032,26.0788312316746,-74.3847796166815));
#6334=CARTESIAN_POINT('Ctrl Pts',(-21.629818783366,26.1383119940679,-74.378614232245));
#6335=CARTESIAN_POINT('Ctrl Pts',(-21.709889671605,26.1977274898354,-74.3724556129175));
#6336=CARTESIAN_POINT('Ctrl Pts',(-21.7928078831468,26.2534884358914,-74.3662969935899));
#6337=CARTESIAN_POINT('Ctrl Pts',(-21.878203809864,26.3053152595329,-74.3601383742624));
#6338=CARTESIAN_POINT('Ctrl Pts',(-21.9424684381944,26.3443174893453,-74.3555037107916));
#6339=CARTESIAN_POINT('Ctrl Pts',(-22.008135510676,26.3810924677873,-74.3508690473208));
#6340=CARTESIAN_POINT('Ctrl Pts',(-22.0750360153461,26.4155367745563,-74.34623438385));
#6341=CARTESIAN_POINT('',(-21.6786659999551,20.9266516823436,-75.));
#6342=CARTESIAN_POINT('Origin',(-23.5502525316942,23.5502525316942,-75.));
#6343=CARTESIAN_POINT('Ctrl Pts',(-21.6786659999559,20.9266516823431,-75.));
#6344=CARTESIAN_POINT('Ctrl Pts',(-21.5953389643838,20.9860943210909,-74.9936814370945));
#6345=CARTESIAN_POINT('Ctrl Pts',(-21.5147913918717,21.049549467126,-74.9873628741889));
#6346=CARTESIAN_POINT('Ctrl Pts',(-21.4374147601277,21.1167295477177,-74.9810443112834));
#6347=CARTESIAN_POINT('Ctrl Pts',(-21.360082230324,21.1838713380423,-74.974729349735));
#6348=CARTESIAN_POINT('Ctrl Pts',(-21.2859173479357,21.2547335710304,-74.9684143881866));
#6349=CARTESIAN_POINT('Ctrl Pts',(-21.2152787784318,21.3289882218752,-74.9620994266382));
#6350=CARTESIAN_POINT('Ctrl Pts',(-21.1446641252583,21.4032177320811,-74.9557866031669));
#6351=CARTESIAN_POINT('Ctrl Pts',(-21.0775736858381,21.4808370797315,-74.9494737796956));
#6352=CARTESIAN_POINT('Ctrl Pts',(-21.0143290622971,21.5614816248623,-74.9431609562242));
#6353=CARTESIAN_POINT('Ctrl Pts',(-20.951073264801,21.6421404181374,-74.9368470174137));
#6354=CARTESIAN_POINT('Ctrl Pts',(-20.891664896588,21.7258251629485,-74.9305330786033));
#6355=CARTESIAN_POINT('Ctrl Pts',(-20.836384932994,21.812138548313,-74.9242191397928));
#6356=CARTESIAN_POINT('Ctrl Pts',(-20.7810964622985,21.8984652165505,-74.9179042293225));
#6357=CARTESIAN_POINT('Ctrl Pts',(-20.7299378798827,21.987420989795,-74.9115893188522));
#6358=CARTESIAN_POINT('Ctrl Pts',(-20.6831459758555,22.0785808427749,-74.9052744083819));
#6359=CARTESIAN_POINT('Ctrl Pts',(-20.6363370244541,22.1697739074002,-74.8989571972435));
#6360=CARTESIAN_POINT('Ctrl Pts',(-20.5938981036181,22.2631722901541,-74.8926399861051));
#6361=CARTESIAN_POINT('Ctrl Pts',(-20.5560190413555,22.3583283026284,-74.8863227749666));
#6362=CARTESIAN_POINT('Ctrl Pts',(-20.5181182037228,22.4535390170214,-74.8800019322808));
#6363=CARTESIAN_POINT('Ctrl Pts',(-20.4847825930215,22.5505089967735,-74.873681089595));
#6364=CARTESIAN_POINT('Ctrl Pts',(-20.4561528862024,22.6487732217445,-74.8673602469092));
#6365=CARTESIAN_POINT('Ctrl Pts',(-20.4274806993935,22.7471832485325,-74.8610300255268));
#6366=CARTESIAN_POINT('Ctrl Pts',(-20.4035284747333,22.8468909664517,-74.8546998041444));
#6367=CARTESIAN_POINT('Ctrl Pts',(-20.3843863356202,22.9474185652856,-74.848369582762));
#6368=CARTESIAN_POINT('Ctrl Pts',(-20.3652284999638,23.0480285966944,-74.8420341706017));
#6369=CARTESIAN_POINT('Ctrl Pts',(-20.3508886683515,23.1494594485779,-74.8356987584413));
#6370=CARTESIAN_POINT('Ctrl Pts',(-20.3414051432903,23.2512274484091,-74.8293633462809));
#6371=CARTESIAN_POINT('Ctrl Pts',(-20.3319048778812,23.3531750894307,-74.8230167508313));
#6372=CARTESIAN_POINT('Ctrl Pts',(-20.3272780627577,23.455460663043,-74.8166701553816));
#6373=CARTESIAN_POINT('Ctrl Pts',(-20.3275109058534,23.5575993386909,-74.8103235599319));
#6374=CARTESIAN_POINT('Ctrl Pts',(-20.3276235433911,23.6070087871021,-74.8072534028297));
#6375=CARTESIAN_POINT('Ctrl Pts',(-20.3288726238348,23.6563839188311,-74.8041832457274));
#6376=CARTESIAN_POINT('Ctrl Pts',(-20.3312522444282,23.7056703977242,-74.8011130886251));
#6377=CARTESIAN_POINT('Ctrl Pts',(-20.3359855990695,23.803707195804,-74.7950061729219));
#6378=CARTESIAN_POINT('Ctrl Pts',(-20.3452120687348,23.9017381762126,-74.7888992572187));
#6379=CARTESIAN_POINT('Ctrl Pts',(-20.3589418227391,23.9993110149775,-74.7827923415155));
#6380=CARTESIAN_POINT('Ctrl Pts',(-20.3726508265874,24.0967363892186,-74.7766946553625));
#6381=CARTESIAN_POINT('Ctrl Pts',(-20.390849534989,24.1937045619621,-74.7705969692095));
#6382=CARTESIAN_POINT('Ctrl Pts',(-20.4134961449647,24.2897638113998,-74.7644992830566));
#6383=CARTESIAN_POINT('Ctrl Pts',(-20.4361155854473,24.3857078170495,-74.7584089123933));
#6384=CARTESIAN_POINT('Ctrl Pts',(-20.4631722242813,24.480744636249,-74.75231854173));
#6385=CARTESIAN_POINT('Ctrl Pts',(-20.4945726794429,24.5744293733799,-74.7462281710667));
#6386=CARTESIAN_POINT('Ctrl Pts',(-20.5259451041581,24.6680304803537,-74.7401432371338));
#6387=CARTESIAN_POINT('Ctrl Pts',(-20.5616534978379,24.7602814841342,-74.7340583032009));
#6388=CARTESIAN_POINT('Ctrl Pts',(-20.6015540524192,24.850750452039,-74.727973369268));
#6389=CARTESIAN_POINT('Ctrl Pts',(-20.6414356065688,24.941176339103,-74.7218913329482));
#6390=CARTESIAN_POINT('Ctrl Pts',(-20.6855051785528,25.0298214690489,-74.7158092966284));
#6391=CARTESIAN_POINT('Ctrl Pts',(-20.7335703639388,25.1162726874868,-74.7097272603086));
#6392=CARTESIAN_POINT('Ctrl Pts',(-20.7816261967079,25.2027070840792,-74.7036464074432));
#6393=CARTESIAN_POINT('Ctrl Pts',(-20.8336758822721,25.2869480285228,-74.6975655545778));
#6394=CARTESIAN_POINT('Ctrl Pts',(-20.8894810127551,25.3686068663888,-74.6914847017125));
#6395=CARTESIAN_POINT('Ctrl Pts',(-20.9452910002887,25.4502728115065,-74.6854033195945));
#6396=CARTESIAN_POINT('Ctrl Pts',(-21.0048568299811,25.5293558370004,-74.6793219374765));
#6397=CARTESIAN_POINT('Ctrl Pts',(-21.0678973721169,25.6054971458995,-74.6732405553586));
#6398=CARTESIAN_POINT('Ctrl Pts',(-21.1310034071258,25.6817175580694,-74.6671528552875));
#6399=CARTESIAN_POINT('Ctrl Pts',(-21.1975910790742,25.7549898072669,-74.6610651552165));
#6400=CARTESIAN_POINT('Ctrl Pts',(-21.2673397998154,25.8249892243964,-74.6549774551454));
#6401=CARTESIAN_POINT('Ctrl Pts',(-21.3371248324939,25.8950250839785,-74.648886585752));
#6402=CARTESIAN_POINT('Ctrl Pts',(-21.4100738611773,25.961784419933,-74.6427957163585));
#6403=CARTESIAN_POINT('Ctrl Pts',(-21.4858320410197,26.0249819310797,-74.6367048469651));
#6404=CARTESIAN_POINT('Ctrl Pts',(-21.5617220540533,26.0882894175399,-74.6306033783366));
#6405=CARTESIAN_POINT('Ctrl Pts',(-21.6404306276229,26.148022430094,-74.6245019097082));
#6406=CARTESIAN_POINT('Ctrl Pts',(-21.721572609624,26.2039381395079,-74.6184004410798));
#6407=CARTESIAN_POINT('Ctrl Pts',(-21.7932718405507,26.2533467595936,-74.6130090198033));
#6408=CARTESIAN_POINT('Ctrl Pts',(-21.8668704763583,26.2997753984595,-74.6076175985267));
#6409=CARTESIAN_POINT('Ctrl Pts',(-21.9420880268178,26.3430870215549,-74.6022261772502));
#6410=CARTESIAN_POINT('Ctrl Pts',(-21.9857916038119,26.3682523299587,-74.5990936052184));
#6411=CARTESIAN_POINT('Ctrl Pts',(-22.0301241723035,26.3924135214964,-74.5959610331866));
#6412=CARTESIAN_POINT('Ctrl Pts',(-22.0750360153461,26.4155367745563,-74.5928284611549));
#6413=CARTESIAN_POINT('Origin',(-23.5502525316942,23.5502525316942,-77.3107734492734));
#6414=CARTESIAN_POINT('',(-22.0750359288953,26.4155367300463,-73.0942273918946));
#6415=CARTESIAN_POINT('',(-22.0750360358082,26.4155367850914,-73.3444460357026));
#6416=CARTESIAN_POINT('',(-22.0750360153461,26.4155367745563,-77.3107734492734));
#6417=CARTESIAN_POINT('',(-26.7730020387288,23.5520350602361,-73.9392265507638));
#6418=CARTESIAN_POINT('Ctrl Pts',(-22.0750359288982,26.4155367300479,-73.0942273918944));
#6419=CARTESIAN_POINT('Ctrl Pts',(-21.9758156807267,26.3644523184142,-73.1006565431777));
#6420=CARTESIAN_POINT('Ctrl Pts',(-21.8791677413006,26.3081726902462,-73.107227114123));
#6421=CARTESIAN_POINT('Ctrl Pts',(-21.7683929477152,26.2356784042351,-73.1152329722461));
#6422=CARTESIAN_POINT('Ctrl Pts',(-21.7513902192451,26.2243187322248,-73.1164754871717));
#6423=CARTESIAN_POINT('Ctrl Pts',(-21.7293242957989,26.2092706067793,-73.1181064454393));
#6424=CARTESIAN_POINT('Ctrl Pts',(-21.7241618682612,26.2057279414766,-73.1184893475809));
#6425=CARTESIAN_POINT('Ctrl Pts',(-21.7162255886803,26.200247660599,-73.1190800573103));
#6426=CARTESIAN_POINT('Ctrl Pts',(-21.7134443895898,26.1983206690126,-73.11928745924));
#6427=CARTESIAN_POINT('Ctrl Pts',(-21.7079761780451,26.1945191848645,-73.119696016041));
#6428=CARTESIAN_POINT('Ctrl Pts',(-21.7052889786307,26.1926449673525,-73.1198971602259));
#6429=CARTESIAN_POINT('Ctrl Pts',(-21.6993781652064,26.1885089917925,-73.1203404195727));
#6430=CARTESIAN_POINT('Ctrl Pts',(-21.6961558329221,26.1862454188536,-73.1205826041859));
#6431=CARTESIAN_POINT('Ctrl Pts',(-21.6894883047369,26.181543444799,-73.1210848430545));
#6432=CARTESIAN_POINT('Ctrl Pts',(-21.6860437358896,26.1791041713051,-73.1213449306176));
#6433=CARTESIAN_POINT('Ctrl Pts',(-21.6772515691842,26.1728520230083,-73.122010393652));
#6434=CARTESIAN_POINT('Ctrl Pts',(-21.6719108358474,26.1690295687906,-73.1224161386826));
#6435=CARTESIAN_POINT('Ctrl Pts',(-21.6565573532798,26.1579696884056,-73.1235869659269));
#6436=CARTESIAN_POINT('Ctrl Pts',(-21.6465745721204,26.1506910365506,-73.124353645096));
#6437=CARTESIAN_POINT('Ctrl Pts',(-21.5498283666167,26.0792957421229,-73.1318371002061));
#6438=CARTESIAN_POINT('Ctrl Pts',(-21.4663035116653,26.0109248873183,-73.1387210661691));
#6439=CARTESIAN_POINT('Ctrl Pts',(-21.1718756290592,25.744157415911,-73.1646304836934));
#6440=CARTESIAN_POINT('Ctrl Pts',(-20.984549395833,25.5218057605228,-73.1846172929653));
#6441=CARTESIAN_POINT('Ctrl Pts',(-20.7758346866239,25.193034785017,-73.2104771321748));
#6442=CARTESIAN_POINT('Ctrl Pts',(-20.7261675010089,25.1061048092495,-73.216998319401));
#6443=CARTESIAN_POINT('Ctrl Pts',(-20.6776338495075,25.0111503905604,-73.2236846544647));
#6444=CARTESIAN_POINT('Ctrl Pts',(-20.6746643105732,25.0052965281475,-73.224095135855));
#6445=CARTESIAN_POINT('Ctrl Pts',(-20.6705875463504,24.9971987625241,-73.2246605404268));
#6446=CARTESIAN_POINT('Ctrl Pts',(-20.6694650446622,24.9949626331997,-73.224816417652));
#6447=CARTESIAN_POINT('Ctrl Pts',(-20.6675455286312,24.991127643746,-73.2250833101893));
#6448=CARTESIAN_POINT('Ctrl Pts',(-20.6667472398382,24.9895294285814,-73.2251944060458));
#6449=CARTESIAN_POINT('Ctrl Pts',(-20.6651907683962,24.9864068002571,-73.2254112117154));
#6450=CARTESIAN_POINT('Ctrl Pts',(-20.6644324668646,24.9848824542151,-73.2255169287173));
#6451=CARTESIAN_POINT('Ctrl Pts',(-20.6625988114931,24.9811890836554,-73.2257727856187));
#6452=CARTESIAN_POINT('Ctrl Pts',(-20.6615246907353,24.9790194421771,-73.2259228472739));
#6453=CARTESIAN_POINT('Ctrl Pts',(-20.658224207919,24.9723337839319,-73.226384525098));
#6454=CARTESIAN_POINT('Ctrl Pts',(-20.6560059697659,24.967813730749,-73.2266956313704));
#6455=CARTESIAN_POINT('Ctrl Pts',(-20.6316796087033,24.9179493291584,-73.2301166109482));
#6456=CARTESIAN_POINT('Ctrl Pts',(-20.6106269767844,24.8720939499548,-73.2331616659311));
#6457=CARTESIAN_POINT('Ctrl Pts',(-20.5516013833588,24.7351352889643,-73.2420160836417));
#6458=CARTESIAN_POINT('Ctrl Pts',(-20.5167242707689,24.6427566831872,-73.2476812271916));
#6459=CARTESIAN_POINT('Ctrl Pts',(-20.378219893922,24.2177957195679,-73.2729773013602));
#6460=CARTESIAN_POINT('Ctrl Pts',(-20.3246889110931,23.8714097868669,-73.2918229258487));
#6461=CARTESIAN_POINT('Ctrl Pts',(-20.3277884887598,23.5026901382269,-73.31412075425));
#6462=CARTESIAN_POINT('Ctrl Pts',(-20.3281556465789,23.4822207587216,-73.315364728141));
#6463=CARTESIAN_POINT('Ctrl Pts',(-20.3288897824493,23.4554958587125,-73.3169972821561));
#6464=CARTESIAN_POINT('Ctrl Pts',(-20.329080015965,23.4492356403689,-73.3173803054869));
#6465=CARTESIAN_POINT('Ctrl Pts',(-20.3294011220676,23.4395944664419,-73.3179711299722));
#6466=CARTESIAN_POINT('Ctrl Pts',(-20.3295190730395,23.4362130715831,-73.3181785249884));
#6467=CARTESIAN_POINT('Ctrl Pts',(-20.3297524439943,23.4298121799517,-73.3185714585507));
#6468=CARTESIAN_POINT('Ctrl Pts',(-20.3298667862271,23.4267926455105,-73.3187569630298));
#6469=CARTESIAN_POINT('Ctrl Pts',(-20.3301359665332,23.4199390903355,-73.3191783371943));
#6470=CARTESIAN_POINT('Ctrl Pts',(-20.3302934054858,23.4161051814898,-73.3194142883652));
#6471=CARTESIAN_POINT('Ctrl Pts',(-20.3307455197778,23.4055550641991,-73.3200642217056));
#6472=CARTESIAN_POINT('Ctrl Pts',(-20.3310543624622,23.3988395104742,-73.3204786486199));
#6473=CARTESIAN_POINT('Ctrl Pts',(-20.3317860880408,23.3839443910274,-73.3213994644717));
#6474=CARTESIAN_POINT('Ctrl Pts',(-20.3322191442286,23.3757653925121,-73.3219061712179));
#6475=CARTESIAN_POINT('Ctrl Pts',(-20.3336299016449,23.3509153883375,-73.3234490138133));
#6476=CARTESIAN_POINT('Ctrl Pts',(-20.3347059957013,23.3342504511807,-73.3244882357131));
#6477=CARTESIAN_POINT('Ctrl Pts',(-20.3390560025035,23.2741518255148,-73.3282528091653));
#6478=CARTESIAN_POINT('Ctrl Pts',(-20.3430807268434,23.2307788011838,-73.3310015357318));
#6479=CARTESIAN_POINT('Ctrl Pts',(-20.3596187397975,23.0847853037168,-73.3403649154961));
#6480=CARTESIAN_POINT('Ctrl Pts',(-20.3761887061833,22.9826972682358,-73.3471009546443));
#6481=CARTESIAN_POINT('Ctrl Pts',(-20.4627888810171,22.5743936805856,-73.3747603954331));
#6482=CARTESIAN_POINT('Ctrl Pts',(-20.5724844447409,22.2783979489563,-73.3966607477543));
#6483=CARTESIAN_POINT('Ctrl Pts',(-20.72525270061,21.9992815394004,-73.4170312838822));
#6484=CARTESIAN_POINT('Ctrl Pts',(-20.7272684533362,21.9956156099976,-73.4172987440077));
#6485=CARTESIAN_POINT('Ctrl Pts',(-20.7320314021978,21.9869933273712,-73.4179275868077));
#6486=CARTESIAN_POINT('Ctrl Pts',(-20.7347845547474,21.982040254456,-73.4182886505243));
#6487=CARTESIAN_POINT('Ctrl Pts',(-20.7388096735962,21.9748436104409,-73.4188129800835));
#6488=CARTESIAN_POINT('Ctrl Pts',(-20.740071274099,21.9725942945982,-73.4189768192117));
#6489=CARTESIAN_POINT('Ctrl Pts',(-20.7488576502879,21.9569729852645,-73.4201143743069));
#6490=CARTESIAN_POINT('Ctrl Pts',(-20.7564753106704,21.9436530620976,-73.4210828434701));
#6491=CARTESIAN_POINT('Ctrl Pts',(-20.7677149967475,21.9243215159098,-73.4224856474612));
#6492=CARTESIAN_POINT('Ctrl Pts',(-20.7712618489792,21.9182667507948,-73.4229246169314));
#6493=CARTESIAN_POINT('Ctrl Pts',(-20.7761357471222,21.9100085732814,-73.4235227371944));
#6494=CARTESIAN_POINT('Ctrl Pts',(-20.7774456628334,21.9077951515272,-73.4236829913666));
#6495=CARTESIAN_POINT('Ctrl Pts',(-20.7796795221479,21.9040307907654,-73.4239554320307));
#6496=CARTESIAN_POINT('Ctrl Pts',(-20.7806021188893,21.9024790604854,-73.4240677065757));
#6497=CARTESIAN_POINT('Ctrl Pts',(-20.7823932632958,21.8994722603002,-73.4242852026202));
#6498=CARTESIAN_POINT('Ctrl Pts',(-20.7832616488853,21.8980171100471,-73.4243904333888));
#6499=CARTESIAN_POINT('Ctrl Pts',(-20.7853466389252,21.8945295544505,-73.4246425758502));
#6500=CARTESIAN_POINT('Ctrl Pts',(-20.7865643360358,21.8924978060167,-73.4247894147454));
#6501=CARTESIAN_POINT('Ctrl Pts',(-20.7902424450221,21.8863761345528,-73.4252316902909));
#6502=CARTESIAN_POINT('Ctrl Pts',(-20.792709717846,21.8822903097043,-73.425526677476));
#6503=CARTESIAN_POINT('Ctrl Pts',(-20.8151569675511,21.8453034139559,-73.4281953413313));
#6504=CARTESIAN_POINT('Ctrl Pts',(-20.8357169037455,21.8127555138264,-73.4305314757884));
#6505=CARTESIAN_POINT('Ctrl Pts',(-20.9049149837808,21.7074376823409,-73.4380770142831));
#6506=CARTESIAN_POINT('Ctrl Pts',(-20.9559375463648,21.6362751017372,-73.4431540398035));
#6507=CARTESIAN_POINT('Ctrl Pts',(-21.0324575601329,21.5382430338127,-73.4502499940243));
#6508=CARTESIAN_POINT('Ctrl Pts',(-21.0556133893881,21.5096032743064,-73.4523360885993));
#6509=CARTESIAN_POINT('Ctrl Pts',(-21.278756091482,21.2430903410978,-73.4719356771536));
#6510=CARTESIAN_POINT('Ctrl Pts',(-21.5116475424034,21.0349442817447,-73.488867576768));
#6511=CARTESIAN_POINT('Ctrl Pts',(-21.7762957243048,20.8596690756067,-73.507847290662));
#6512=CARTESIAN_POINT('Ctrl Pts',(-21.7818704208894,20.8560018384863,-73.5082468871696));
#6513=CARTESIAN_POINT('Ctrl Pts',(-21.7980654700034,20.8454200662502,-73.5094072096528));
#6514=CARTESIAN_POINT('Ctrl Pts',(-21.8087151834232,20.838550884582,-73.5101695504745));
#6515=CARTESIAN_POINT('Ctrl Pts',(-21.8225413072594,20.8297479257202,-73.5111585160949));
#6516=CARTESIAN_POINT('Ctrl Pts',(-21.8256810355493,20.8277565187179,-73.5113830470236));
#6517=CARTESIAN_POINT('Ctrl Pts',(-21.8468217371978,20.8143990426028,-73.5128945578803));
#6518=CARTESIAN_POINT('Ctrl Pts',(-21.8649311713159,20.803206361008,-73.5141877821618));
#6519=CARTESIAN_POINT('Ctrl Pts',(-21.888592963779,20.7889040395359,-73.5158759820131));
#6520=CARTESIAN_POINT('Ctrl Pts',(-21.8940457864662,20.7856300925655,-73.5162649202174));
#6521=CARTESIAN_POINT('Ctrl Pts',(-21.9027560427582,20.7804353569413,-73.5168860514657));
#6522=CARTESIAN_POINT('Ctrl Pts',(-21.9060072468433,20.7785041113529,-73.5171178620881));
#6523=CARTESIAN_POINT('Ctrl Pts',(-21.9120990431188,20.7749000175487,-73.5175521468133));
#6524=CARTESIAN_POINT('Ctrl Pts',(-21.9149388201346,20.7732257953155,-73.5177545704775));
#6525=CARTESIAN_POINT('Ctrl Pts',(-21.92130682989,20.7694846190779,-73.5182084401133));
#6526=CARTESIAN_POINT('Ctrl Pts',(-21.9248364331385,20.767420019743,-73.5184599713082));
#6527=CARTESIAN_POINT('Ctrl Pts',(-21.935169392448,20.7614022436365,-73.5191962342525));
#6528=CARTESIAN_POINT('Ctrl Pts',(-21.9419832724265,20.7574672796902,-73.5196816255655));
#6529=CARTESIAN_POINT('Ctrl Pts',(-21.957425478504,20.7486247775465,-73.5207814135541));
#6530=CARTESIAN_POINT('Ctrl Pts',(-21.9660621746895,20.7437320875481,-73.5213963417332));
#6531=CARTESIAN_POINT('Ctrl Pts',(-21.993605107078,20.7282966581067,-73.5233569115272));
#6532=CARTESIAN_POINT('Ctrl Pts',(-22.0125947170841,20.7179046425228,-73.5247079361831));
#6533=CARTESIAN_POINT('Ctrl Pts',(-22.0861374788476,20.6786161228805,-73.5299382934159));
#6534=CARTESIAN_POINT('Ctrl Pts',(-22.1414090614959,20.6510995881107,-73.5338656045585));
#6535=CARTESIAN_POINT('Ctrl Pts',(-22.3070265689111,20.5745028126027,-73.5456280499296));
#6536=CARTESIAN_POINT('Ctrl Pts',(-22.4193705535818,20.5300210816243,-73.5536040486037));
#6537=CARTESIAN_POINT('Ctrl Pts',(-22.8057419635218,20.401624396989,-73.5808957826998));
#6538=CARTESIAN_POINT('Ctrl Pts',(-23.0883788894103,20.3479346347013,-73.6007436413631));
#6539=CARTESIAN_POINT('Ctrl Pts',(-23.3747803484998,20.3322831060708,-73.6188898450561));
#6540=CARTESIAN_POINT('Ctrl Pts',(-23.3751655524019,20.3322621244672,-73.6189142475701));
#6541=CARTESIAN_POINT('Ctrl Pts',(-23.3910216990411,20.3314013142865,-73.6199185737069));
#6542=CARTESIAN_POINT('Ctrl Pts',(-23.4064988663177,20.3306729745878,-73.6208928436122));
#6543=CARTESIAN_POINT('Ctrl Pts',(-23.4255073462744,20.32991580152,-73.6220814816862));
#6544=CARTESIAN_POINT('Ctrl Pts',(-23.4290338915378,20.3297811285349,-73.6223016688528));
#6545=CARTESIAN_POINT('Ctrl Pts',(-23.4348667689977,20.3295679750413,-73.6226652951191));
#6546=CARTESIAN_POINT('Ctrl Pts',(-23.4371729645218,20.3294861789059,-73.6228089200425));
#6547=CARTESIAN_POINT('Ctrl Pts',(-23.4411581608415,20.3293491176179,-73.6230568563884));
#6548=CARTESIAN_POINT('Ctrl Pts',(-23.442837112724,20.32929268836,-73.6231612335248));
#6549=CARTESIAN_POINT('Ctrl Pts',(-23.446611706597,20.3291687795872,-73.6233957175267));
#6550=CARTESIAN_POINT('Ctrl Pts',(-23.4487073667277,20.329102032533,-73.6235257823563));
#6551=CARTESIAN_POINT('Ctrl Pts',(-23.4543029990669,20.3289292770869,-73.6238727494713));
#6552=CARTESIAN_POINT('Ctrl Pts',(-23.4578030939631,20.3288269272102,-73.6240894452205));
#6553=CARTESIAN_POINT('Ctrl Pts',(-23.4742454541612,20.3283729386707,-73.6251058754951));
#6554=CARTESIAN_POINT('Ctrl Pts',(-23.4871898339757,20.3280935819665,-73.6259015891815));
#6555=CARTESIAN_POINT('Ctrl Pts',(-23.5900685676046,20.3264935294867,-73.6321926174568));
#6556=CARTESIAN_POINT('Ctrl Pts',(-23.6800299149093,20.3288601996525,-73.6374930202744));
#6557=CARTESIAN_POINT('Ctrl Pts',(-23.852083778636,20.3406076196147,-73.6474434596173));
#6558=CARTESIAN_POINT('Ctrl Pts',(-23.934142371661,20.3493850890063,-73.6521073160595));
#6559=CARTESIAN_POINT('Ctrl Pts',(-24.041179294247,20.3650103897594,-73.6581805730917));
#6560=CARTESIAN_POINT('Ctrl Pts',(-24.0665364940799,20.3690220349133,-73.6596185219087));
#6561=CARTESIAN_POINT('Ctrl Pts',(-24.1137511356775,20.3770710378569,-73.6622983138799));
#6562=CARTESIAN_POINT('Ctrl Pts',(-24.135619908862,20.3810323583784,-73.6635404818334));
#6563=CARTESIAN_POINT('Ctrl Pts',(-24.176679781833,20.3889094600406,-73.6658769452275));
#6564=CARTESIAN_POINT('Ctrl Pts',(-24.1958795269183,20.3927745984768,-73.6669712295623));
#6565=CARTESIAN_POINT('Ctrl Pts',(-24.2809569264454,20.410710143665,-73.6718317355551));
#6566=CARTESIAN_POINT('Ctrl Pts',(-24.3464181684235,20.4266687986296,-73.67560277403));
#6567=CARTESIAN_POINT('Ctrl Pts',(-24.5486780689916,20.4827488726202,-73.6874501815381));
#6568=CARTESIAN_POINT('Ctrl Pts',(-24.6833342008178,20.5298963212732,-73.6956293085145));
#6569=CARTESIAN_POINT('Ctrl Pts',(-24.8215061499554,20.5888185621005,-73.7045608070273));
#6570=CARTESIAN_POINT('Ctrl Pts',(-24.8285820367175,20.5918660469175,-73.7050197010606));
#6571=CARTESIAN_POINT('Ctrl Pts',(-24.8469398306658,20.5998506493155,-73.7062142422856));
#6572=CARTESIAN_POINT('Ctrl Pts',(-24.8582044135229,20.6048270806791,-73.7069511476958));
#6573=CARTESIAN_POINT('Ctrl Pts',(-24.8762213105506,20.6129102634189,-73.7081362211176));
#6574=CARTESIAN_POINT('Ctrl Pts',(-24.8829919496606,20.6159760542795,-73.7085830322922));
#6575=CARTESIAN_POINT('Ctrl Pts',(-24.915060668055,20.6306308759748,-73.7107063889694));
#6576=CARTESIAN_POINT('Ctrl Pts',(-24.9402179642565,20.6425235410514,-73.7123930381376));
#6577=CARTESIAN_POINT('Ctrl Pts',(-24.970908673687,20.6575213287143,-73.7144775583137));
#6578=CARTESIAN_POINT('Ctrl Pts',(-24.9765915892829,20.6603192144065,-73.7148646847351));
#6579=CARTESIAN_POINT('Ctrl Pts',(-24.9859807654453,20.6649762548078,-73.7155061915969));
#6580=CARTESIAN_POINT('Ctrl Pts',(-24.9896917704035,20.6668258492618,-73.7157602369089));
#6581=CARTESIAN_POINT('Ctrl Pts',(-24.9962194126344,20.6700950203113,-73.7162079768247));
#6582=CARTESIAN_POINT('Ctrl Pts',(-24.9990375603495,20.6715115826363,-73.7164015653749));
#6583=CARTESIAN_POINT('Ctrl Pts',(-25.0046583750909,20.6743472700287,-73.7167882561897));
#6584=CARTESIAN_POINT('Ctrl Pts',(-25.0074610557714,20.6757663604581,-73.7169813570767));
#6585=CARTESIAN_POINT('Ctrl Pts',(-25.015173889584,20.6796858038294,-73.7175135545716));
#6586=CARTESIAN_POINT('Ctrl Pts',(-25.0200796953421,20.6821946465869,-73.7178529501426));
#6587=CARTESIAN_POINT('Ctrl Pts',(-25.0395440322177,20.6922118190374,-73.7192030898002));
#6588=CARTESIAN_POINT('Ctrl Pts',(-25.0540514631789,20.6998184162532,-73.7202173029757));
#6589=CARTESIAN_POINT('Ctrl Pts',(-25.0903016001945,20.7191790047341,-73.7227717516774));
#6590=CARTESIAN_POINT('Ctrl Pts',(-25.1119679597188,20.7310729851955,-73.724316937074));
#6591=CARTESIAN_POINT('Ctrl Pts',(-25.1974933075352,20.779311506939,-73.7304911496828));
#6592=CARTESIAN_POINT('Ctrl Pts',(-25.2602339928692,20.8175838100533,-73.7351886257889));
#6593=CARTESIAN_POINT('Ctrl Pts',(-25.4432632974591,20.9380055362176,-73.7494078992253));
#6594=CARTESIAN_POINT('Ctrl Pts',(-25.5593410104589,21.0261923772822,-73.7591289353105));
#6595=CARTESIAN_POINT('Ctrl Pts',(-25.8547327084271,21.2839303624163,-73.7855927189618));
#6596=CARTESIAN_POINT('Ctrl Pts',(-26.0212363053244,21.466720601368,-73.8024933888385));
#6597=CARTESIAN_POINT('Ctrl Pts',(-26.1736443642566,21.6783184171562,-73.8189690473407));
#6598=CARTESIAN_POINT('Ctrl Pts',(-26.1819245423139,21.6899771534297,-73.8198676343764));
#6599=CARTESIAN_POINT('Ctrl Pts',(-26.1922831929323,21.7047700262716,-73.8209958191519));
#6600=CARTESIAN_POINT('Ctrl Pts',(-26.1944339828318,21.7078529695617,-73.8212302896136));
#6601=CARTESIAN_POINT('Ctrl Pts',(-26.1978211373298,21.7127262666405,-73.8215998872281));
#6602=CARTESIAN_POINT('Ctrl Pts',(-26.1990610827548,21.7145141090956,-73.8217352599974));
#6603=CARTESIAN_POINT('Ctrl Pts',(-26.2013596783686,21.7178355671272,-73.8219863461941));
#6604=CARTESIAN_POINT('Ctrl Pts',(-26.2024188039935,21.7193688381454,-73.82210209212));
#6605=CARTESIAN_POINT('Ctrl Pts',(-26.2047740677519,21.7227848297524,-73.8223596035649));
#6606=CARTESIAN_POINT('Ctrl Pts',(-26.2060695299175,21.7246680063816,-73.8225013222168));
#6607=CARTESIAN_POINT('Ctrl Pts',(-26.2098408952567,21.7301628435182,-73.8229141339957));
#6608=CARTESIAN_POINT('Ctrl Pts',(-26.2123114549546,21.7337781921479,-73.8231848611488));
#6609=CARTESIAN_POINT('Ctrl Pts',(-26.2299039826636,21.7596355865177,-73.8251149153877));
#6610=CARTESIAN_POINT('Ctrl Pts',(-26.2447549459512,21.7820619884561,-73.8267560748414));
#6611=CARTESIAN_POINT('Ctrl Pts',(-26.2853806495699,21.8451114826825,-73.8312871398988));
#6612=CARTESIAN_POINT('Ctrl Pts',(-26.3105300767433,21.8861310771874,-73.8341407406226));
#6613=CARTESIAN_POINT('Ctrl Pts',(-26.5046048529728,22.2191874854402,-73.8566928070685));
#6614=CARTESIAN_POINT('Ctrl Pts',(-26.6276479308132,22.5355504961937,-73.8745957281164));
#6615=CARTESIAN_POINT('Ctrl Pts',(-26.7033217867866,22.8834558309663,-73.8953095069888));
#6616=CARTESIAN_POINT('Ctrl Pts',(-26.7071178503884,22.9016656764101,-73.8963957567001));
#6617=CARTESIAN_POINT('Ctrl Pts',(-26.7143921840814,22.9381386272106,-73.8985763867742));
#6618=CARTESIAN_POINT('Ctrl Pts',(-26.7178704842886,22.9564009855831,-73.8996707198113));
#6619=CARTESIAN_POINT('Ctrl Pts',(-26.7223738108325,22.9812111880614,-73.9011612828438));
#6620=CARTESIAN_POINT('Ctrl Pts',(-26.7235369736599,22.9877338121914,-73.9015535141595));
#6621=CARTESIAN_POINT('Ctrl Pts',(-26.7271998051643,23.0086466682404,-73.9028122953579));
#6622=CARTESIAN_POINT('Ctrl Pts',(-26.7296217401929,23.0230501836991,-73.9036811000038));
#6623=CARTESIAN_POINT('Ctrl Pts',(-26.7390577233955,23.0815981481341,-73.907220744086));
#6624=CARTESIAN_POINT('Ctrl Pts',(-26.7452506696875,23.1258681834554,-73.9099159264471));
#6625=CARTESIAN_POINT('Ctrl Pts',(-26.7513987888541,23.1776459588676,-73.9130944818731));
#6626=CARTESIAN_POINT('Ctrl Pts',(-26.752251221644,23.1850438161157,-73.9135492459722));
#6627=CARTESIAN_POINT('Ctrl Pts',(-26.7535703423128,23.1968515818765,-73.9142761118865));
#6628=CARTESIAN_POINT('Ctrl Pts',(-26.7540535854108,23.2012596448741,-73.914547690016));
#6629=CARTESIAN_POINT('Ctrl Pts',(-26.7548902851022,23.2090400907829,-73.9150274412236));
#6630=CARTESIAN_POINT('Ctrl Pts',(-26.7552475209327,23.2124120675446,-73.9152354945338));
#6631=CARTESIAN_POINT('Ctrl Pts',(-26.7559241559984,23.2188965458795,-73.9156358501233));
#6632=CARTESIAN_POINT('Ctrl Pts',(-26.7562443456957,23.2220089626036,-73.9158281271736));
#6633=CARTESIAN_POINT('Ctrl Pts',(-26.7569178894717,23.2286511789244,-73.9162387125626));
#6634=CARTESIAN_POINT('Ctrl Pts',(-26.7572699487036,23.2321811030639,-73.9164570615696));
#6635=CARTESIAN_POINT('Ctrl Pts',(-26.7580997164055,23.240642217053,-73.9169807959942));
#6636=CARTESIAN_POINT('Ctrl Pts',(-26.7585718825053,23.2455739302734,-73.9172863561342));
#6637=CARTESIAN_POINT('Ctrl Pts',(-26.7598069076893,23.2587948786291,-73.9181062943876));
#6638=CARTESIAN_POINT('Ctrl Pts',(-26.7605490216312,23.2670859718664,-73.9186213263913));
#6639=CARTESIAN_POINT('Ctrl Pts',(-26.7691406263219,23.367451317547,-73.9248661657328));
#6640=CARTESIAN_POINT('Ctrl Pts',(-26.7730577462239,23.4598091419467,-73.9307192919354));
#6641=CARTESIAN_POINT('Ctrl Pts',(-26.7730019438629,23.5521990328162,-73.9366887153694));
#6642=CARTESIAN_POINT('Ctrl Pts',(-22.0750360153461,26.4155367745563,-74.34623438385));
#6643=CARTESIAN_POINT('Ctrl Pts',(-22.1638502850276,26.46126357386,-74.3400816013948));
#6644=CARTESIAN_POINT('Ctrl Pts',(-22.2548390451486,26.5028809965016,-74.3339288189396));
#6645=CARTESIAN_POINT('Ctrl Pts',(-22.3475842422765,26.540186736343,-74.3277760364844));
#6646=CARTESIAN_POINT('Ctrl Pts',(-22.4403129201626,26.5774858315003,-74.3216243499274));
#6647=CARTESIAN_POINT('Ctrl Pts',(-22.5347970105746,26.6104746083562,-74.3154726633705));
#6648=CARTESIAN_POINT('Ctrl Pts',(-22.6305982685655,26.6389988143806,-74.3093209768136));
#6649=CARTESIAN_POINT('Ctrl Pts',(-22.726408047016,26.6675255573168,-74.3031687431323));
#6650=CARTESIAN_POINT('Ctrl Pts',(-22.8235348095442,26.691586817123,-74.2970165094511));
#6651=CARTESIAN_POINT('Ctrl Pts',(-22.9215259051911,26.7110784350976,-74.2908642757698));
#6652=CARTESIAN_POINT('Ctrl Pts',(-23.0199097668309,26.7306481789941,-74.2846873828259));
#6653=CARTESIAN_POINT('Ctrl Pts',(-23.1191644739776,26.7456114804933,-74.278510489882));
#6654=CARTESIAN_POINT('Ctrl Pts',(-23.2188238826832,26.7559151173564,-74.272333596938));
#6655=CARTESIAN_POINT('Ctrl Pts',(-23.3182371317515,26.7661933041437,-74.2661719609753));
#6656=CARTESIAN_POINT('Ctrl Pts',(-23.4180526475076,26.7718348372567,-74.2600103250126));
#6657=CARTESIAN_POINT('Ctrl Pts',(-23.5178062923391,26.7728391952382,-74.2538486890499));
#6658=CARTESIAN_POINT('Ctrl Pts',(-23.61793044092,26.7738472835937,-74.2476641676153));
#6659=CARTESIAN_POINT('Ctrl Pts',(-23.717991819053,26.7701837123499,-74.2414796461808));
#6660=CARTESIAN_POINT('Ctrl Pts',(-23.8175262436563,26.761900445989,-74.2352951247462));
#6661=CARTESIAN_POINT('Ctrl Pts',(-23.9170606682595,26.753617179628,-74.2291106033117));
#6662=CARTESIAN_POINT('Ctrl Pts',(-24.0160677153349,26.7407143351953,-74.2229260818772));
#6663=CARTESIAN_POINT('Ctrl Pts',(-24.1140948251003,26.7232951457583,-74.2167415604426));
#6664=CARTESIAN_POINT('Ctrl Pts',(-24.2119463802174,26.705907151974,-74.2105681147349));
#6665=CARTESIAN_POINT('Ctrl Pts',(-24.3091642918956,26.6839580768627,-74.2043946690271));
#6666=CARTESIAN_POINT('Ctrl Pts',(-24.40529055219,26.6575065518874,-74.1982212233194));
#6667=CARTESIAN_POINT('Ctrl Pts',(-24.5012870325805,26.6310907390719,-74.1920561123704));
#6668=CARTESIAN_POINT('Ctrl Pts',(-24.5961943760753,26.6001846729129,-74.1858910014214));
#6669=CARTESIAN_POINT('Ctrl Pts',(-24.6895630872402,26.5648982854307,-74.1797258904724));
#6670=CARTESIAN_POINT('Ctrl Pts',(-24.7828332965206,26.5296491242915,-74.1735672835764));
#6671=CARTESIAN_POINT('Ctrl Pts',(-24.874567696709,26.4900289818559,-74.1674086766804));
#6672=CARTESIAN_POINT('Ctrl Pts',(-24.9643312583758,26.4461977862262,-74.1612500697845));
#6673=CARTESIAN_POINT('Ctrl Pts',(-25.0540297073452,26.4023983848717,-74.1550959302191));
#6674=CARTESIAN_POINT('Ctrl Pts',(-25.1417597711075,26.3543941933535,-74.1489417906537));
#6675=CARTESIAN_POINT('Ctrl Pts',(-25.2271065991256,26.3023931529268,-74.1427876510884));
#6676=CARTESIAN_POINT('Ctrl Pts',(-25.3124213477109,26.2504116582047,-74.1366358246881));
#6677=CARTESIAN_POINT('Ctrl Pts',(-25.3953542701286,26.1944365253345,-74.1304839982879));
#6678=CARTESIAN_POINT('Ctrl Pts',(-25.4755161133061,26.1347210851533,-74.1243321718877));
#6679=CARTESIAN_POINT('Ctrl Pts',(-25.5556692449119,26.0750121345351,-74.1181810140359));
#6680=CARTESIAN_POINT('Ctrl Pts',(-25.6330515478184,26.0115639441327,-74.1120298561841));
#6681=CARTESIAN_POINT('Ctrl Pts',(-25.7073045326274,25.9446719243174,-74.1058786983323));
#6682=CARTESIAN_POINT('Ctrl Pts',(-25.7815692879801,25.8777693008147,-74.0997265654023));
#6683=CARTESIAN_POINT('Ctrl Pts',(-25.852703417293,25.8074220541724,-74.0935744324723));
#6684=CARTESIAN_POINT('Ctrl Pts',(-25.92038392367,25.7339637642684,-74.0874222995422));
#6685=CARTESIAN_POINT('Ctrl Pts',(-25.9881370002476,25.6604267089544,-74.0812635700078));
#6686=CARTESIAN_POINT('Ctrl Pts',(-26.052428764335,25.5837722690493,-74.0751048404735));
#6687=CARTESIAN_POINT('Ctrl Pts',(-26.1129753969161,25.5043684644293,-74.0689461109391));
#6688=CARTESIAN_POINT('Ctrl Pts',(-26.1735559143592,25.4249202215499,-74.062783934678));
#6689=CARTESIAN_POINT('Ctrl Pts',(-26.2303868792733,25.3427199068222,-74.0566217584168));
#6690=CARTESIAN_POINT('Ctrl Pts',(-26.2832280450616,25.258164240722,-74.0504595821557));
#6691=CARTESIAN_POINT('Ctrl Pts',(-26.3361576398668,25.1734670717931,-74.0442870935711));
#6692=CARTESIAN_POINT('Ctrl Pts',(-26.3850838858273,25.0864070568192,-74.0381146049866));
#6693=CARTESIAN_POINT('Ctrl Pts',(-26.4298126296483,24.99740532417,-74.0319421164021));
#6694=CARTESIAN_POINT('Ctrl Pts',(-26.463840758868,24.9296957888544,-74.0272462939573));
#6695=CARTESIAN_POINT('Ctrl Pts',(-26.4954404739716,24.8608629589719,-74.0225504715125));
#6696=CARTESIAN_POINT('Ctrl Pts',(-26.524545431243,24.7910987390034,-74.0178546490678));
#6697=CARTESIAN_POINT('Ctrl Pts',(-26.5671860774408,24.6888896413158,-74.0109749652528));
#6698=CARTESIAN_POINT('Ctrl Pts',(-26.604598155147,24.5843757468685,-74.0040952814378));
#6699=CARTESIAN_POINT('Ctrl Pts',(-26.6365541860418,24.4780777635515,-73.9972155976228));
#6700=CARTESIAN_POINT('Ctrl Pts',(-26.6684132457932,24.3721023433531,-73.9903567903306));
#6701=CARTESIAN_POINT('Ctrl Pts',(-26.694849181671,24.2643538679654,-73.9834979830383));
#6702=CARTESIAN_POINT('Ctrl Pts',(-26.7156828145406,24.1553712695786,-73.9766391757461));
#6703=CARTESIAN_POINT('Ctrl Pts',(-26.7364026540635,24.0469839343746,-73.9698178312738));
#6704=CARTESIAN_POINT('Ctrl Pts',(-26.7515811121171,23.937376159783,-73.9629964868015));
#6705=CARTESIAN_POINT('Ctrl Pts',(-26.7610895711912,23.8270973768584,-73.9561751423292));
#6706=CARTESIAN_POINT('Ctrl Pts',(-26.7689646066732,23.7357629848532,-73.9505256118074));
#6707=CARTESIAN_POINT('Ctrl Pts',(-26.7729511894786,23.6439687332407,-73.9448760812856));
#6708=CARTESIAN_POINT('Ctrl Pts',(-26.7730020387288,23.5520350602361,-73.9392265507638));
#6709=CARTESIAN_POINT('',(-26.7730019206732,23.5522370557033,-74.1857734492731));
#6710=CARTESIAN_POINT('Ctrl Pts',(-22.0750360153461,26.4155367745563,-74.5928284611549));
#6711=CARTESIAN_POINT('Ctrl Pts',(-22.1636076089027,26.4611386299462,-74.5866506497362));
#6712=CARTESIAN_POINT('Ctrl Pts',(-22.2544338538382,26.5027009229343,-74.5804728383175));
#6713=CARTESIAN_POINT('Ctrl Pts',(-22.3471109305284,26.5399963083487,-74.5742950268988));
#6714=CARTESIAN_POINT('Ctrl Pts',(-22.4396766330714,26.5772468742468,-74.5681246396297));
#6715=CARTESIAN_POINT('Ctrl Pts',(-22.5340883468709,26.6102405661368,-74.5619542523606));
#6716=CARTESIAN_POINT('Ctrl Pts',(-22.6299185416649,26.6387963486566,-74.5557838650914));
#6717=CARTESIAN_POINT('Ctrl Pts',(-22.7285671015863,26.6681919564717,-74.5494320067907));
#6718=CARTESIAN_POINT('Ctrl Pts',(-22.8287184657271,26.6928843316223,-74.5430801484901));
#6719=CARTESIAN_POINT('Ctrl Pts',(-22.9298848592266,26.7127296483635,-74.5367282901894));
#6720=CARTESIAN_POINT('Ctrl Pts',(-23.0280174924835,26.7319798471921,-74.5305669103126));
#6721=CARTESIAN_POINT('Ctrl Pts',(-23.1271046867706,26.7466694756759,-74.5244055304357));
#6722=CARTESIAN_POINT('Ctrl Pts',(-23.2266879909635,26.7567184289839,-74.5182441505589));
#6723=CARTESIAN_POINT('Ctrl Pts',(-23.3262472978702,26.7667649607253,-74.5120842554329));
#6724=CARTESIAN_POINT('Ctrl Pts',(-23.4263020466877,26.7721729965736,-74.5059243603069));
#6725=CARTESIAN_POINT('Ctrl Pts',(-23.5263874747349,26.772914167913,-74.499764465181));
#6726=CARTESIAN_POINT('Ctrl Pts',(-23.626475309744,26.7736553570768,-74.4936044219152));
#6727=CARTESIAN_POINT('Ctrl Pts',(-23.726593392647,26.7697294562033,-74.4874443786495));
#6728=CARTESIAN_POINT('Ctrl Pts',(-23.8262767533552,26.7611602213602,-74.4812843353837));
#6729=CARTESIAN_POINT('Ctrl Pts',(-23.9259889296083,26.752588509402,-74.4751225114296));
#6730=CARTESIAN_POINT('Ctrl Pts',(-24.0252657029357,26.7393708335459,-74.4689606874755));
#6731=CARTESIAN_POINT('Ctrl Pts',(-24.1236480019802,26.7215827253441,-74.4627988635213));
#6732=CARTESIAN_POINT('Ctrl Pts',(-24.222140422206,26.7037747065739,-74.4566301425203));
#6733=CARTESIAN_POINT('Ctrl Pts',(-24.3197359439699,26.6813861237143,-74.4504614215192));
#6734=CARTESIAN_POINT('Ctrl Pts',(-24.415986659057,26.6545434303085,-74.4442927005181));
#6735=CARTESIAN_POINT('Ctrl Pts',(-24.5123022205314,26.6276826523441,-74.4381198235036));
#6736=CARTESIAN_POINT('Ctrl Pts',(-24.6072707614017,26.5963619250118,-74.431946946489));
#6737=CARTESIAN_POINT('Ctrl Pts',(-24.7004623612232,26.5607566274488,-74.4257740694744));
#6738=CARTESIAN_POINT('Ctrl Pts',(-24.7937922583881,26.5250984912385,-74.4195920318435));
#6739=CARTESIAN_POINT('Ctrl Pts',(-24.8853395574873,26.4851432701484,-74.4134099942126));
#6740=CARTESIAN_POINT('Ctrl Pts',(-24.9746972375318,26.4411131029621,-74.4072279565817));
#6741=CARTESIAN_POINT('Ctrl Pts',(-24.9934334752511,26.4318809957855,-74.4059317263462));
#6742=CARTESIAN_POINT('Ctrl Pts',(-25.0120735458385,26.422469890201,-74.4046354961108));
#6743=CARTESIAN_POINT('Ctrl Pts',(-25.0306138588376,26.412882075243,-74.4033392658753));
#6744=CARTESIAN_POINT('Ctrl Pts',(-25.1190531126965,26.3671471838704,-74.3971561105609));
#6745=CARTESIAN_POINT('Ctrl Pts',(-25.2055203593367,26.3172327871667,-74.3909729552464));
#6746=CARTESIAN_POINT('Ctrl Pts',(-25.289595062973,26.2633329067264,-74.384789799932));
#6747=CARTESIAN_POINT('Ctrl Pts',(-25.3735589558713,26.2095040665071,-74.3786147940367));
#6748=CARTESIAN_POINT('Ctrl Pts',(-25.4551362129971,26.1517004159409,-74.3724397881414));
#6749=CARTESIAN_POINT('Ctrl Pts',(-25.5339298493267,26.0901623454494,-74.3662647822462));
#6750=CARTESIAN_POINT('Ctrl Pts',(-25.6126426733369,26.0286873896261,-74.3600961095597));
#6751=CARTESIAN_POINT('Ctrl Pts',(-25.6885772138999,25.963485894204,-74.3539274368732));
#6752=CARTESIAN_POINT('Ctrl Pts',(-25.7613653037703,25.8948415941232,-74.3477587641867));
#6753=CARTESIAN_POINT('Ctrl Pts',(-25.834103221162,25.8262446102269,-74.3415943435365));
#6754=CARTESIAN_POINT('Ctrl Pts',(-25.903698686081,25.7542098358229,-74.3354299228863));
#6755=CARTESIAN_POINT('Ctrl Pts',(-25.9698171759252,25.6790607651636,-74.3292655022361));
#6756=CARTESIAN_POINT('Ctrl Pts',(-26.0359122357238,25.6039383246672,-74.3231032660377));
#6757=CARTESIAN_POINT('Ctrl Pts',(-26.0985324834489,25.5257041054362,-74.3169410298394));
#6758=CARTESIAN_POINT('Ctrl Pts',(-26.1573814203929,25.4447172371486,-74.310778793641));
#6759=CARTESIAN_POINT('Ctrl Pts',(-26.2162250839103,25.3637376260579,-74.3046171096378));
#6760=CARTESIAN_POINT('Ctrl Pts',(-26.2712978543429,25.2800062063495,-74.2984554256346));
#6761=CARTESIAN_POINT('Ctrl Pts',(-26.3223451800199,25.1939130536994,-74.2922937416315));
#6762=CARTESIAN_POINT('Ctrl Pts',(-26.3734014461824,25.1078048225987,-74.2861309784641));
#6763=CARTESIAN_POINT('Ctrl Pts',(-26.420430646287,25.0193344088958,-74.2799682152967));
#6764=CARTESIAN_POINT('Ctrl Pts',(-26.4632235061485,24.928917706596,-74.2738054521294));
#6765=CARTESIAN_POINT('Ctrl Pts',(-26.5060628376104,24.8384028148112,-74.2676359964094));
#6766=CARTESIAN_POINT('Ctrl Pts',(-26.5446564567202,24.7459378055551,-74.2614665406893));
#6767=CARTESIAN_POINT('Ctrl Pts',(-26.5788427587947,24.6519597517899,-74.2552970849693));
#6768=CARTESIAN_POINT('Ctrl Pts',(-26.613048546435,24.5579281322562,-74.2491241127726));
#6769=CARTESIAN_POINT('Ctrl Pts',(-26.6428418851251,24.4623821635771,-74.2429511405758));
#6770=CARTESIAN_POINT('Ctrl Pts',(-26.668111315878,24.3657733250454,-74.2367781683791));
#6771=CARTESIAN_POINT('Ctrl Pts',(-26.6934229705998,24.2690030579229,-74.2305948814511));
#6772=CARTESIAN_POINT('Ctrl Pts',(-26.7141955280556,24.1711667967266,-74.2244115945232));
#6773=CARTESIAN_POINT('Ctrl Pts',(-26.7303687981163,24.0727255879733,-74.2182283075952));
#6774=CARTESIAN_POINT('Ctrl Pts',(-26.7423797890527,23.9996187603704,-74.2136363232303));
#6775=CARTESIAN_POINT('Ctrl Pts',(-26.7518552545503,23.9261784765462,-74.2090443388653));
#6776=CARTESIAN_POINT('Ctrl Pts',(-26.7587891415197,23.8525940371305,-74.2044523545004));
#6777=CARTESIAN_POINT('Ctrl Pts',(-26.7681908443758,23.752820412715,-74.1982260527579));
#6778=CARTESIAN_POINT('Ctrl Pts',(-26.7729401209426,23.6525961559481,-74.1919997510155));
#6779=CARTESIAN_POINT('Ctrl Pts',(-26.7730019206732,23.5522370557033,-74.1857734492731));
#6780=CARTESIAN_POINT('Ctrl Pts',(-26.7730018334319,23.552374005015,-74.1834084018853));
#6781=CARTESIAN_POINT('Ctrl Pts',(-26.7731731936204,23.2920591934439,-74.1683346339349));
#6782=CARTESIAN_POINT('Ctrl Pts',(-26.7418053767837,23.0326559172775,-74.1542544132757));
#6783=CARTESIAN_POINT('Ctrl Pts',(-26.6527383336224,22.6708854196747,-74.1330410158101));
#6784=CARTESIAN_POINT('Ctrl Pts',(-26.6202498266327,22.5634305571839,-74.126542358643));
#6785=CARTESIAN_POINT('Ctrl Pts',(-26.5653829434107,22.4111406508839,-74.1169029855998));
#6786=CARTESIAN_POINT('Ctrl Pts',(-26.5474598812864,22.3647842864118,-74.1139099833266));
#6787=CARTESIAN_POINT('Ctrl Pts',(-26.5254646687034,22.3115870046156,-74.110400313905));
#6788=CARTESIAN_POINT('Ctrl Pts',(-26.5224297838194,22.304322385826,-74.1099193972657));
#6789=CARTESIAN_POINT('Ctrl Pts',(-26.5177769187787,22.293298545438,-74.1091871040994));
#6790=CARTESIAN_POINT('Ctrl Pts',(-26.5161783321312,22.2895311280677,-74.1089363934697));
#6791=CARTESIAN_POINT('Ctrl Pts',(-26.5132694580615,22.2827118865635,-74.1084817763106));
#6792=CARTESIAN_POINT('Ctrl Pts',(-26.5119616190123,22.2796590188185,-74.108277954225));
#6793=CARTESIAN_POINT('Ctrl Pts',(-26.5093390270982,22.2735631946185,-74.1078703754233));
#6794=CARTESIAN_POINT('Ctrl Pts',(-26.5080242938307,22.2705202340388,-74.1076666195734));
#6795=CARTESIAN_POINT('Ctrl Pts',(-26.5043159139954,22.2619734011992,-74.107093485947));
#6796=CARTESIAN_POINT('Ctrl Pts',(-26.5019115929895,22.256474200677,-74.1067237401197));
#6797=CARTESIAN_POINT('Ctrl Pts',(-26.4919945701673,22.2339633618703,-74.1052061459204));
#6798=CARTESIAN_POINT('Ctrl Pts',(-26.4843501687463,22.2170104560567,-74.1040537468586));
#6799=CARTESIAN_POINT('Ctrl Pts',(-26.4697159119018,22.1852917284274,-74.1018793990026));
#6800=CARTESIAN_POINT('Ctrl Pts',(-26.4627596453122,22.1705109906939,-74.1008586515998));
#6801=CARTESIAN_POINT('Ctrl Pts',(-26.4500719660861,22.1440756316,-74.0990193529368));
#6802=CARTESIAN_POINT('Ctrl Pts',(-26.444381869436,22.1324014835075,-74.0982022600768));
#6803=CARTESIAN_POINT('Ctrl Pts',(-26.4348968024971,22.1132363506917,-74.0968528165984));
#6804=CARTESIAN_POINT('Ctrl Pts',(-26.4311428017041,22.105725161394,-74.0963218949798));
#6805=CARTESIAN_POINT('Ctrl Pts',(-26.4255063987995,22.0945569320732,-74.0955294108137));
#6806=CARTESIAN_POINT('Ctrl Pts',(-26.4236462600132,22.0908886425752,-74.0952686183662));
#6807=CARTESIAN_POINT('Ctrl Pts',(-26.4176360100783,22.0790921592347,-74.094428365001));
#6808=CARTESIAN_POINT('Ctrl Pts',(-26.4134584202331,22.0709780843051,-74.093847960863));
#6809=CARTESIAN_POINT('Ctrl Pts',(-26.3982162032591,22.0416798007035,-74.0917433489619));
#6810=CARTESIAN_POINT('Ctrl Pts',(-26.3869506828606,22.0206014897318,-74.0902123179817));
#6811=CARTESIAN_POINT('Ctrl Pts',(-26.2296131837086,21.7339322389166,-74.0691570833579));
#6812=CARTESIAN_POINT('Ctrl Pts',(-26.0470256099903,21.490142246053,-74.048285803409));
#6813=CARTESIAN_POINT('Ctrl Pts',(-25.7919426967307,21.2341456103311,-74.0241051369264));
#6814=CARTESIAN_POINT('Ctrl Pts',(-25.7496156218093,21.1939145352312,-74.020232262364));
#6815=CARTESIAN_POINT('Ctrl Pts',(-25.6729775439087,21.1249368906135,-74.01349354921));
#6816=CARTESIAN_POINT('Ctrl Pts',(-25.6391171446194,21.0957133648934,-74.0106049306079));
#6817=CARTESIAN_POINT('Ctrl Pts',(-25.5878132502417,21.0532659800151,-74.0063718181071));
#6818=CARTESIAN_POINT('Ctrl Pts',(-25.5708269651545,21.0395007431033,-74.0049929260526));
#6819=CARTESIAN_POINT('Ctrl Pts',(-25.5504859041213,21.0233570313041,-74.0033697458957));
#6820=CARTESIAN_POINT('Ctrl Pts',(-25.5472655582968,21.0208112127281,-74.0031135936597));
#6821=CARTESIAN_POINT('Ctrl Pts',(-25.5426073722957,21.0171431621158,-74.0027442746002));
#6822=CARTESIAN_POINT('Ctrl Pts',(-25.5411734471658,21.0160160002134,-74.002630751439));
#6823=CARTESIAN_POINT('Ctrl Pts',(-25.5383238722555,21.0137799532882,-74.0024054787508));
#6824=CARTESIAN_POINT('Ctrl Pts',(-25.5369082550465,21.0126710388054,-74.0022937274034));
#6825=CARTESIAN_POINT('Ctrl Pts',(-25.5340799319032,21.0104593077088,-74.002070772594));
#6826=CARTESIAN_POINT('Ctrl Pts',(-25.5326672323665,21.0093564832459,-74.0019595685063));
#6827=CARTESIAN_POINT('Ctrl Pts',(-25.5292647387224,21.0067048901377,-74.0016921111418));
#6828=CARTESIAN_POINT('Ctrl Pts',(-25.5272740416981,21.0051572742396,-74.001535940698));
#6829=CARTESIAN_POINT('Ctrl Pts',(-25.5211600438974,21.0004156066549,-74.0010572426436));
#6830=CARTESIAN_POINT('Ctrl Pts',(-25.5170307777783,20.9972292067746,-74.0007352576979));
#6831=CARTESIAN_POINT('Ctrl Pts',(-25.4697915624277,20.9609591019028,-73.9970665033251));
#6832=CARTESIAN_POINT('Ctrl Pts',(-25.4258560569786,20.9289584175873,-73.9937945995209));
#6833=CARTESIAN_POINT('Ctrl Pts',(-25.3705114997343,20.8907523325541,-73.9898149133693));
#6834=CARTESIAN_POINT('Ctrl Pts',(-25.359849831816,20.8834863926253,-73.989054607345));
#6835=CARTESIAN_POINT('Ctrl Pts',(-25.2689269212389,20.8223186778309,-73.9826218083097));
#6836=CARTESIAN_POINT('Ctrl Pts',(-25.1863155876713,20.7719859818886,-73.9771126591773));
#6837=CARTESIAN_POINT('Ctrl Pts',(-25.0401320728113,20.6917060354189,-73.9677147371931));
#6838=CARTESIAN_POINT('Ctrl Pts',(-24.9776182704327,20.6599832627997,-73.9638000600999));
#6839=CARTESIAN_POINT('Ctrl Pts',(-24.7735165411243,20.564649596152,-73.9512135054993));
#6840=CARTESIAN_POINT('Ctrl Pts',(-24.6283596435621,20.5092196871638,-73.9425435688092));
#6841=CARTESIAN_POINT('Ctrl Pts',(-24.4006048966428,20.4406132568563,-73.9288150233273));
#6842=CARTESIAN_POINT('Ctrl Pts',(-24.3205437188905,20.4198203859502,-73.9239689592116));
#6843=CARTESIAN_POINT('Ctrl Pts',(-24.1983389395987,20.3930542528631,-73.9164892662991));
#6844=CARTESIAN_POINT('Ctrl Pts',(-24.1567283199703,20.3847977742896,-73.9139284032327));
#6845=CARTESIAN_POINT('Ctrl Pts',(-24.1074783869251,20.3760321888643,-73.9108771049625));
#6846=CARTESIAN_POINT('Ctrl Pts',(-24.0999838147574,20.3747256536103,-73.9104122272031));
#6847=CARTESIAN_POINT('Ctrl Pts',(-24.0884803473159,20.3727621881554,-73.9096978189052));
#6848=CARTESIAN_POINT('Ctrl Pts',(-24.0844746836128,20.3720862747228,-73.9094488916634));
#6849=CARTESIAN_POINT('Ctrl Pts',(-24.07716074237,20.370866342397,-73.9089940784488));
#6850=CARTESIAN_POINT('Ctrl Pts',(-24.0738528688596,20.3703199082009,-73.9087882694578));
#6851=CARTESIAN_POINT('Ctrl Pts',(-24.0671947451766,20.3692307101382,-73.9083737896306));
#6852=CARTESIAN_POINT('Ctrl Pts',(-24.0638444785661,20.3686880748171,-73.9081651150007));
#6853=CARTESIAN_POINT('Ctrl Pts',(-24.0542903969377,20.3671561054015,-73.9075696994322));
#6854=CARTESIAN_POINT('Ctrl Pts',(-24.048084563035,20.3661796216691,-73.9071825516606));
#6855=CARTESIAN_POINT('Ctrl Pts',(-24.0215830601376,20.3620889994941,-73.9055275454476));
#6856=CARTESIAN_POINT('Ctrl Pts',(-24.0012610883809,20.3591507743765,-73.9042541320727));
#6857=CARTESIAN_POINT('Ctrl Pts',(-23.6414538441664,20.3106341251809,-73.8816279678724));
#6858=CARTESIAN_POINT('Ctrl Pts',(-23.2969308663212,20.3192851419755,-73.8583524628253));
#6859=CARTESIAN_POINT('Ctrl Pts',(-22.8594984343816,20.4007283300809,-73.8284146377176));
#6860=CARTESIAN_POINT('Ctrl Pts',(-22.7595796870382,20.4243152825993,-73.821577723196));
#6861=CARTESIAN_POINT('Ctrl Pts',(-22.6282540538186,20.4620178446651,-73.8127274999079));
#6862=CARTESIAN_POINT('Ctrl Pts',(-22.5957075908082,20.4719220035411,-73.8105456776735));
#6863=CARTESIAN_POINT('Ctrl Pts',(-22.5520730251936,20.4859589939648,-73.8076417242578));
#6864=CARTESIAN_POINT('Ctrl Pts',(-22.5408432183487,20.4896398380281,-73.8068962700496));
#6865=CARTESIAN_POINT('Ctrl Pts',(-22.5244855442217,20.49510129026,-73.8058134688052));
#6866=CARTESIAN_POINT('Ctrl Pts',(-22.5193416802277,20.4968331635176,-73.805473410805));
#6867=CARTESIAN_POINT('Ctrl Pts',(-22.5101273883393,20.4999614363531,-73.8048650827754));
#6868=CARTESIAN_POINT('Ctrl Pts',(-22.506055351018,20.501353004236,-73.8045965357065));
#6869=CARTESIAN_POINT('Ctrl Pts',(-22.4998441667246,20.5034895018634,-73.8041873686863));
#6870=CARTESIAN_POINT('Ctrl Pts',(-22.4977030177515,20.5042285308176,-73.8040464012964));
#6871=CARTESIAN_POINT('Ctrl Pts',(-22.4937986512272,20.5055807520359,-73.8037895015613));
#6872=CARTESIAN_POINT('Ctrl Pts',(-22.4920351857257,20.5061932194986,-73.803673526039));
#6873=CARTESIAN_POINT('Ctrl Pts',(-22.4882251015333,20.5075202070863,-73.8034230777163));
#6874=CARTESIAN_POINT('Ctrl Pts',(-22.4861786743836,20.5082352589158,-73.8032886372789));
#6875=CARTESIAN_POINT('Ctrl Pts',(-22.4806259882158,20.51018173808,-73.80292405862));
#6876=CARTESIAN_POINT('Ctrl Pts',(-22.4771211214997,20.5114171709872,-73.8026941591273));
#6877=CARTESIAN_POINT('Ctrl Pts',(-22.4605794734741,20.5172801349079,-73.8016101405867));
#6878=CARTESIAN_POINT('Ctrl Pts',(-22.4475701836713,20.5219856033909,-73.8007606025528));
#6879=CARTESIAN_POINT('Ctrl Pts',(-22.244104145818,20.5970644316854,-73.7875148789264));
#6880=CARTESIAN_POINT('Ctrl Pts',(-22.0606530356323,20.6852108778867,-73.7761229725251));
#6881=CARTESIAN_POINT('Ctrl Pts',(-21.7638912434107,20.8640674739802,-73.756744722397));
#6882=CARTESIAN_POINT('Ctrl Pts',(-21.646164762407,20.9461932788097,-73.7487658703992));
#6883=CARTESIAN_POINT('Ctrl Pts',(-21.4270915312859,21.1218399115396,-73.7327358188833));
#6884=CARTESIAN_POINT('Ctrl Pts',(-21.3255009291452,21.2145569770672,-73.7247179945337));
#6885=CARTESIAN_POINT('Ctrl Pts',(-21.2151169684542,21.3290528024566,-73.7151043032376));
#6886=CARTESIAN_POINT('Ctrl Pts',(-21.2002474724256,21.3447905570142,-73.7137888743219));
#6887=CARTESIAN_POINT('Ctrl Pts',(-21.1813736392967,21.3651740608185,-73.7120922530703));
#6888=CARTESIAN_POINT('Ctrl Pts',(-21.1772221842605,21.3696833170005,-73.711717366033));
#6889=CARTESIAN_POINT('Ctrl Pts',(-21.1705643161092,21.3769565369993,-73.7111133855583));
#6890=CARTESIAN_POINT('Ctrl Pts',(-21.1680497812854,21.3797130734696,-73.7108846377599));
#6891=CARTESIAN_POINT('Ctrl Pts',(-21.1632768923156,21.384963594933,-73.7104492295681));
#6892=CARTESIAN_POINT('Ctrl Pts',(-21.1610176441365,21.3874567635766,-73.710242607455));
#6893=CARTESIAN_POINT('Ctrl Pts',(-21.1558859809618,21.3931376077002,-73.7097720939159));
#6894=CARTESIAN_POINT('Ctrl Pts',(-21.1530160241333,21.3963274863137,-73.7095080992428));
#6895=CARTESIAN_POINT('Ctrl Pts',(-21.1443201213155,21.4060316529311,-73.7087055976501));
#6896=CARTESIAN_POINT('Ctrl Pts',(-21.1385143307542,21.4125638761718,-73.7081662451342));
#6897=CARTESIAN_POINT('Ctrl Pts',(-21.0976820853821,21.4588832105907,-73.7043475318647));
#6898=CARTESIAN_POINT('Ctrl Pts',(-21.063617146124,21.4995035587788,-73.7010284498143));
#6899=CARTESIAN_POINT('Ctrl Pts',(-21.0278066659131,21.5444100467975,-73.6973877640093));
#6900=CARTESIAN_POINT('Ctrl Pts',(-21.0250495383985,21.5478821707593,-73.6971064524718));
#6901=CARTESIAN_POINT('Ctrl Pts',(-21.018266294329,21.5564607817363,-73.6964118609188));
#6902=CARTESIAN_POINT('Ctrl Pts',(-21.0142484643566,21.5615737698344,-73.695998263067));
#6903=CARTESIAN_POINT('Ctrl Pts',(-21.0039040382932,21.574820151016,-73.6949277414588));
#6904=CARTESIAN_POINT('Ctrl Pts',(-20.9976009617988,21.5829717435713,-73.6942699296701));
#6905=CARTESIAN_POINT('Ctrl Pts',(-20.9872567245945,21.5964830695988,-73.6931811865302));
#6906=CARTESIAN_POINT('Ctrl Pts',(-20.9831929904259,21.6018254920664,-73.6927510997639));
#6907=CARTESIAN_POINT('Ctrl Pts',(-20.8772262041948,21.7420425799459,-73.6814736374));
#6908=CARTESIAN_POINT('Ctrl Pts',(-20.786088388299,21.8846967975081,-73.67023454867));
#6909=CARTESIAN_POINT('Ctrl Pts',(-20.6294657304119,22.1784032059693,-73.6477753594769));
#6910=CARTESIAN_POINT('Ctrl Pts',(-20.5635030056395,22.3286570098561,-73.6366003936102));
#6911=CARTESIAN_POINT('Ctrl Pts',(-20.4857445451581,22.5502775715763,-73.6210187343627));
#6912=CARTESIAN_POINT('Ctrl Pts',(-20.4644556141968,22.6180411500755,-73.6163715925069));
#6913=CARTESIAN_POINT('Ctrl Pts',(-20.4401615155956,22.7053640457343,-73.610576864214));
#6914=CARTESIAN_POINT('Ctrl Pts',(-20.435074213302,22.7243186538684,-73.6093305482742));
#6915=CARTESIAN_POINT('Ctrl Pts',(-20.428186704274,22.7509499254413,-73.607596696327));
#6916=CARTESIAN_POINT('Ctrl Pts',(-20.4262411546113,22.7585880787836,-73.6071013853896));
#6917=CARTESIAN_POINT('Ctrl Pts',(-20.423344100896,22.7701387966519,-73.6063554221177));
#6918=CARTESIAN_POINT('Ctrl Pts',(-20.422371892099,22.7740460649213,-73.6061036136483));
#6919=CARTESIAN_POINT('Ctrl Pts',(-20.4206000450068,22.7812244344559,-73.6056419792606));
#6920=CARTESIAN_POINT('Ctrl Pts',(-20.4197982078921,22.7844949795886,-73.605432028118));
#6921=CARTESIAN_POINT('Ctrl Pts',(-20.418516376307,22.7897589947419,-73.6050947163301));
#6922=CARTESIAN_POINT('Ctrl Pts',(-20.4180331583697,22.7917516654239,-73.6049671687204));
#6923=CARTESIAN_POINT('Ctrl Pts',(-20.4171119860626,22.7955662426078,-73.6047232741843));
#6924=CARTESIAN_POINT('Ctrl Pts',(-20.4166737220293,22.7973880569998,-73.6046069101104));
#6925=CARTESIAN_POINT('Ctrl Pts',(-20.4156760752098,22.8015511257531,-73.604341272812));
#6926=CARTESIAN_POINT('Ctrl Pts',(-20.4151177274076,22.8038926212885,-73.6041920604894));
#6927=CARTESIAN_POINT('Ctrl Pts',(-20.4136717905408,22.8099865758389,-73.6038042211352));
#6928=CARTESIAN_POINT('Ctrl Pts',(-20.4127883088303,22.8137400187149,-73.6035658319005));
#6929=CARTESIAN_POINT('Ctrl Pts',(-20.4073772073704,22.8369153285242,-73.6020969038803));
#6930=CARTESIAN_POINT('Ctrl Pts',(-20.4030230767316,22.8563778490695,-73.6008762390203));
#6931=CARTESIAN_POINT('Ctrl Pts',(-20.3972964150641,22.8831390524395,-73.5992139530539));
#6932=CARTESIAN_POINT('Ctrl Pts',(-20.3957681350738,22.8904034115707,-73.5987643501517));
#6933=CARTESIAN_POINT('Ctrl Pts',(-20.3929826225252,22.9038746336809,-73.5979334973003));
#6934=CARTESIAN_POINT('Ctrl Pts',(-20.3917185631697,22.9100800257116,-73.5975519118949));
#6935=CARTESIAN_POINT('Ctrl Pts',(-20.3556743053576,23.0897306488406,-73.5865366203628));
#6936=CARTESIAN_POINT('Ctrl Pts',(-20.3352106074342,23.2657667413021,-73.5765925619934));
#6937=CARTESIAN_POINT('Ctrl Pts',(-20.3240454113311,23.5998654555163,-73.5578950111063));
#6938=CARTESIAN_POINT('Ctrl Pts',(-20.3303135582794,23.7572895311376,-73.5491548076088));
#6939=CARTESIAN_POINT('Ctrl Pts',(-20.362713992734,24.0428208619325,-73.5327085040281));
#6940=CARTESIAN_POINT('Ctrl Pts',(-20.3851791635773,24.1710020138349,-73.5251037329687));
#6941=CARTESIAN_POINT('Ctrl Pts',(-20.4185226257497,24.3108943111876,-73.5164077662797));
#6942=CARTESIAN_POINT('Ctrl Pts',(-20.4218094327274,24.3243015532919,-73.5155703324412));
#6943=CARTESIAN_POINT('Ctrl Pts',(-20.427712554048,24.3477291112185,-73.5140997978857));
#6944=CARTESIAN_POINT('Ctrl Pts',(-20.4302912370297,24.3577587686641,-73.5134679171008));
#6945=CARTESIAN_POINT('Ctrl Pts',(-20.434083898284,24.3722207351997,-73.5125533776723));
#6946=CARTESIAN_POINT('Ctrl Pts',(-20.4352591046716,24.3766632217766,-73.5122719789936));
#6947=CARTESIAN_POINT('Ctrl Pts',(-20.4373215804574,24.38439283631,-73.5117815465301));
#6948=CARTESIAN_POINT('Ctrl Pts',(-20.4382045670207,24.38768110798,-73.5115726523618));
#6949=CARTESIAN_POINT('Ctrl Pts',(-20.4399169954336,24.394018137354,-73.5111695790786));
#6950=CARTESIAN_POINT('Ctrl Pts',(-20.4407457135376,24.3970670882169,-73.5109754237381));
#6951=CARTESIAN_POINT('Ctrl Pts',(-20.4427156825568,24.4042729507486,-73.5105160274139));
#6952=CARTESIAN_POINT('Ctrl Pts',(-20.4438607908298,24.4084287938441,-73.5102506608692));
#6953=CARTESIAN_POINT('Ctrl Pts',(-20.4472887751136,24.4207729205915,-73.5094611893633));
#6954=CARTESIAN_POINT('Ctrl Pts',(-20.4495957003912,24.4289544347353,-73.50893630005));
#6955=CARTESIAN_POINT('Ctrl Pts',(-20.4710094267654,24.5037638383739,-73.5041216907847));
#6956=CARTESIAN_POINT('Ctrl Pts',(-20.492227406454,24.5697637077898,-73.4997631113147));
#6957=CARTESIAN_POINT('Ctrl Pts',(-20.5188236003766,24.6441677387285,-73.4947160399268));
#6958=CARTESIAN_POINT('Ctrl Pts',(-20.5221332328792,24.6532962093144,-73.4940945131101));
#6959=CARTESIAN_POINT('Ctrl Pts',(-20.5841168297762,24.8218749577686,-73.4825736640319));
#6960=CARTESIAN_POINT('Ctrl Pts',(-20.6552603631311,24.9764331059884,-73.4712780980678));
#6961=CARTESIAN_POINT('Ctrl Pts',(-20.8295286715011,25.2876921481589,-73.4472084338869));
#6962=CARTESIAN_POINT('Ctrl Pts',(-20.9348248520234,25.4424939465576,-73.4344429208427));
#6963=CARTESIAN_POINT('Ctrl Pts',(-21.0961741495497,25.6402989949978,-73.4176740415605));
#6964=CARTESIAN_POINT('Ctrl Pts',(-21.1410830942451,25.6919105714252,-73.4132537704316));
#6965=CARTESIAN_POINT('Ctrl Pts',(-21.1925584229928,25.7473982061385,-73.4084872928207));
#6966=CARTESIAN_POINT('Ctrl Pts',(-21.1975307190187,25.7527217595166,-73.4080298436341));
#6967=CARTESIAN_POINT('Ctrl Pts',(-21.2051249552495,25.7607974102057,-73.4073357477571));
#6968=CARTESIAN_POINT('Ctrl Pts',(-21.2077337444805,25.7635617603417,-73.4070981251452));
#6969=CARTESIAN_POINT('Ctrl Pts',(-21.2120029816633,25.7680695667169,-73.4067105981867));
#6970=CARTESIAN_POINT('Ctrl Pts',(-21.2136604941682,25.7698157791186,-73.4065604706438));
#6971=CARTESIAN_POINT('Ctrl Pts',(-21.2168570882644,25.7731758863011,-73.4062715765223));
#6972=CARTESIAN_POINT('Ctrl Pts',(-21.2183958904462,25.7747900433169,-73.4061327884906));
#6973=CARTESIAN_POINT('Ctrl Pts',(-21.2211986716251,25.7777239723194,-73.4058805143548));
#6974=CARTESIAN_POINT('Ctrl Pts',(-21.2224620912472,25.7790442598073,-73.4057669858953));
#6975=CARTESIAN_POINT('Ctrl Pts',(-21.2250322014036,25.78172548417,-73.405536426412));
#6976=CARTESIAN_POINT('Ctrl Pts',(-21.2263389589364,25.7830863428913,-73.4054194016712));
#6977=CARTESIAN_POINT('Ctrl Pts',(-21.2300743839009,25.7869695870701,-73.4050854544928));
#6978=CARTESIAN_POINT('Ctrl Pts',(-21.2325059777905,25.7894891729297,-73.404868760672));
#6979=CARTESIAN_POINT('Ctrl Pts',(-21.2429536235344,25.8002796370593,-73.4039406403197));
#6980=CARTESIAN_POINT('Ctrl Pts',(-21.251010006268,25.8085116056728,-73.4032323311843));
#6981=CARTESIAN_POINT('Ctrl Pts',(-21.3922155024301,25.9512556148662,-73.3909418399778));
#6982=CARTESIAN_POINT('Ctrl Pts',(-21.536938042602,26.0738466826071,-73.3802472402356));
#6983=CARTESIAN_POINT('Ctrl Pts',(-21.8138821578065,26.2693586443004,-73.3612607451901));
#6984=CARTESIAN_POINT('Ctrl Pts',(-21.9420042342511,26.3470442060735,-73.3529587830562));
#6985=CARTESIAN_POINT('Ctrl Pts',(-22.0750360358082,26.4155367850914,-73.3444460357026));
#6986=CARTESIAN_POINT('Origin',(-23.5502525316942,23.5502525316942,-77.3107734492734));
#6987=CARTESIAN_POINT('',(-22.0750359824043,26.4155367575959,-71.8489552970435));
#6988=CARTESIAN_POINT('',(-22.0750360205127,26.4155367772164,-72.0953994964366));
#6989=CARTESIAN_POINT('',(-22.0750360153461,26.4155367745563,-77.3107734492734));
#6990=CARTESIAN_POINT('Ctrl Pts',(-22.0750359824043,26.4155367575959,-71.8489552970435));
#6991=CARTESIAN_POINT('Ctrl Pts',(-21.9777291534232,26.3654374888483,-71.8553412661841));
#6992=CARTESIAN_POINT('Ctrl Pts',(-21.8830050340865,26.3103970587655,-71.8615301479144));
#6993=CARTESIAN_POINT('Ctrl Pts',(-21.6716115338078,26.1726957195411,-71.8756798750198));
#6994=CARTESIAN_POINT('Ctrl Pts',(-21.5572972618043,26.0869095881927,-71.8835940046763));
#6995=CARTESIAN_POINT('Ctrl Pts',(-21.3160947428769,25.8795020721675,-71.9016071275874));
#6996=CARTESIAN_POINT('Ctrl Pts',(-21.1927128203315,25.7545341372085,-71.9117715040743));
#6997=CARTESIAN_POINT('Ctrl Pts',(-21.0715695807337,25.6099674165137,-71.9232295631562));
#6998=CARTESIAN_POINT('Ctrl Pts',(-21.0630875385045,25.599717063337,-71.9240403537687));
#6999=CARTESIAN_POINT('Ctrl Pts',(-21.0514487236261,25.5854731581692,-71.9251649049877));
#7000=CARTESIAN_POINT('Ctrl Pts',(-21.0482374943415,25.5815241093113,-71.9254764571077));
#7001=CARTESIAN_POINT('Ctrl Pts',(-21.0428325947734,25.5748451048418,-71.9260030137902));
#7002=CARTESIAN_POINT('Ctrl Pts',(-21.0406339871695,25.5721191415714,-71.926217818704));
#7003=CARTESIAN_POINT('Ctrl Pts',(-21.0362924530504,25.5667182598519,-71.9266432044628));
#7004=CARTESIAN_POINT('Ctrl Pts',(-21.0341493414999,25.5640434955213,-71.9268537774642));
#7005=CARTESIAN_POINT('Ctrl Pts',(-21.0294356578141,25.5581411928867,-71.9273182291355));
#7006=CARTESIAN_POINT('Ctrl Pts',(-21.0268670116346,25.5549121298034,-71.9275721846476));
#7007=CARTESIAN_POINT('Ctrl Pts',(-21.0179197566787,25.5436200287897,-71.9284597945172));
#7008=CARTESIAN_POINT('Ctrl Pts',(-21.0115735870028,25.5355314727357,-71.929094743219));
#7009=CARTESIAN_POINT('Ctrl Pts',(-20.947076924091,25.4525118381883,-71.9356034220269));
#7010=CARTESIAN_POINT('Ctrl Pts',(-20.8922280604317,25.3750858285623,-71.9416066058685));
#7011=CARTESIAN_POINT('Ctrl Pts',(-20.6944986942914,25.0681001448142,-71.9651949418541));
#7012=CARTESIAN_POINT('Ctrl Pts',(-20.5773115792254,24.823347305175,-71.9836804191454));
#7013=CARTESIAN_POINT('Ctrl Pts',(-20.4666212653899,24.4903796442771,-72.0072705451087));
#7014=CARTESIAN_POINT('Ctrl Pts',(-20.4440613567244,24.4129220786975,-72.0126455682629));
#7015=CARTESIAN_POINT('Ctrl Pts',(-20.4147584566119,24.2961568345057,-72.020509570936));
#7016=CARTESIAN_POINT('Ctrl Pts',(-20.4058000343932,24.2574407161664,-72.0230784833591));
#7017=CARTESIAN_POINT('Ctrl Pts',(-20.3939415007324,24.2014995100962,-72.0267257059563));
#7018=CARTESIAN_POINT('Ctrl Pts',(-20.3904620636705,24.1844024984702,-72.0278317614911));
#7019=CARTESIAN_POINT('Ctrl Pts',(-20.3857378469712,24.160184171031,-72.0293855297584));
#7020=CARTESIAN_POINT('Ctrl Pts',(-20.3843779882386,24.1530859845995,-72.0298393529876));
#7021=CARTESIAN_POINT('Ctrl Pts',(-20.3823431850721,24.14226792485,-72.0305285496676));
#7022=CARTESIAN_POINT('Ctrl Pts',(-20.381650899973,24.1385513961735,-72.0307648810856));
#7023=CARTESIAN_POINT('Ctrl Pts',(-20.3805298232945,24.1324735155421,-72.0311506386431));
#7024=CARTESIAN_POINT('Ctrl Pts',(-20.3800971294116,24.130112900788,-72.0313002846857));
#7025=CARTESIAN_POINT('Ctrl Pts',(-20.3792683836582,24.125562922286,-72.031588370905));
#7026=CARTESIAN_POINT('Ctrl Pts',(-20.3788719615023,24.1233736285842,-72.0317268321561));
#7027=CARTESIAN_POINT('Ctrl Pts',(-20.3781687280862,24.119466857948,-72.0319736343711));
#7028=CARTESIAN_POINT('Ctrl Pts',(-20.3778610452337,24.1177495475479,-72.0320820251874));
#7029=CARTESIAN_POINT('Ctrl Pts',(-20.3772268812357,24.1141933725559,-72.0323062784514));
#7030=CARTESIAN_POINT('Ctrl Pts',(-20.3769006050758,24.1123544800355,-72.0324221287565));
#7031=CARTESIAN_POINT('Ctrl Pts',(-20.3759834211874,24.1071589803208,-72.0327491354142));
#7032=CARTESIAN_POINT('Ctrl Pts',(-20.3753962371025,24.1038017051077,-72.0329600781));
#7033=CARTESIAN_POINT('Ctrl Pts',(-20.3729775816292,24.0898423864206,-72.0338356682477));
#7034=CARTESIAN_POINT('Ctrl Pts',(-20.3711938545097,24.0792319777876,-72.0344976169819));
#7035=CARTESIAN_POINT('Ctrl Pts',(-20.3401319842542,23.888628460456,-72.0463277098167));
#7036=CARTESIAN_POINT('Ctrl Pts',(-20.3261253554334,23.7064489255816,-72.0566676403883));
#7037=CARTESIAN_POINT('Ctrl Pts',(-20.3289657225009,23.3572673473885,-72.0762462254496));
#7038=CARTESIAN_POINT('Ctrl Pts',(-20.3432654359956,23.1908583874367,-72.0854778049068));
#7039=CARTESIAN_POINT('Ctrl Pts',(-20.3880039481781,22.9193370622962,-72.1011787405092));
#7040=CARTESIAN_POINT('Ctrl Pts',(-20.4110137617024,22.8133352814155,-72.1074702243302));
#7041=CARTESIAN_POINT('Ctrl Pts',(-20.4520811771191,22.6615228375527,-72.1168424069214));
#7042=CARTESIAN_POINT('Ctrl Pts',(-20.4659144919076,22.6146432805094,-72.1197873257624));
#7043=CARTESIAN_POINT('Ctrl Pts',(-20.4832105835241,22.5605892511582,-72.1232482174252));
#7044=CARTESIAN_POINT('Ctrl Pts',(-20.4856408279504,22.5530891427696,-72.1237298930721));
#7045=CARTESIAN_POINT('Ctrl Pts',(-20.4893809463424,22.5416893839822,-72.1244642792005));
#7046=CARTESIAN_POINT('Ctrl Pts',(-20.4906708185243,22.5377831617258,-72.1247163284514));
#7047=CARTESIAN_POINT('Ctrl Pts',(-20.4930234644322,22.5307040091725,-72.1251738516152));
#7048=CARTESIAN_POINT('Ctrl Pts',(-20.4940837091341,22.527530239298,-72.1253792415711));
#7049=CARTESIAN_POINT('Ctrl Pts',(-20.49621411608,22.52118590791,-72.1257903571472));
#7050=CARTESIAN_POINT('Ctrl Pts',(-20.4972842774074,22.5180153504142,-72.1259960825283));
#7051=CARTESIAN_POINT('Ctrl Pts',(-20.5003118511548,22.5090914779391,-72.1265758876328));
#7052=CARTESIAN_POINT('Ctrl Pts',(-20.5022805943097,22.5033420470909,-72.1269503429847));
#7053=CARTESIAN_POINT('Ctrl Pts',(-20.5104606266446,22.4796720993922,-72.1284956901964));
#7054=CARTESIAN_POINT('Ctrl Pts',(-20.5168136933384,22.4618013030087,-72.129671288589));
#7055=CARTESIAN_POINT('Ctrl Pts',(-20.5257780582922,22.4372732726301,-72.1312972975468));
#7056=CARTESIAN_POINT('Ctrl Pts',(-20.5282544118218,22.4305668465466,-72.1317431702275));
#7057=CARTESIAN_POINT('Ctrl Pts',(-20.5312044853172,22.4226585779567,-72.1322704820308));
#7058=CARTESIAN_POINT('Ctrl Pts',(-20.5316566540999,22.4214486698116,-72.1323511994399));
#7059=CARTESIAN_POINT('Ctrl Pts',(-20.5357117980481,22.4106178219614,-72.1330741460223));
#7060=CARTESIAN_POINT('Ctrl Pts',(-20.539359997375,22.4010139797499,-72.1337178842916));
#7061=CARTESIAN_POINT('Ctrl Pts',(-20.5469034077748,22.3814385145636,-72.1350355611625));
#7062=CARTESIAN_POINT('Ctrl Pts',(-20.5508025066026,22.3714685356557,-72.1357096229055));
#7063=CARTESIAN_POINT('Ctrl Pts',(-20.5572984607302,22.3550993268493,-72.1368212321806));
#7064=CARTESIAN_POINT('Ctrl Pts',(-20.5598663606759,22.3486886337079,-72.1372578152524));
#7065=CARTESIAN_POINT('Ctrl Pts',(-20.564660582047,22.3368305510708,-72.1380676888874));
#7066=CARTESIAN_POINT('Ctrl Pts',(-20.5668812614038,22.3313808995148,-72.1384407918372));
#7067=CARTESIAN_POINT('Ctrl Pts',(-20.5736315613165,22.3149443144508,-72.1395688480641));
#7068=CARTESIAN_POINT('Ctrl Pts',(-20.5782070027763,22.3039764142392,-72.1403253000523));
#7069=CARTESIAN_POINT('Ctrl Pts',(-20.5881904122782,22.280412595688,-72.1419585326713));
#7070=CARTESIAN_POINT('Ctrl Pts',(-20.5936182765269,22.267825405309,-72.1428359461744));
#7071=CARTESIAN_POINT('Ctrl Pts',(-20.7019342245609,22.0209843318913,-72.160140838154));
#7072=CARTESIAN_POINT('Ctrl Pts',(-20.8322636547231,21.7998030102599,-72.1775039521415));
#7073=CARTESIAN_POINT('Ctrl Pts',(-21.0914865460765,21.4597736467118,-72.2063861223673));
#7074=CARTESIAN_POINT('Ctrl Pts',(-21.2064159121376,21.3316767577781,-72.2178761529594));
#7075=CARTESIAN_POINT('Ctrl Pts',(-21.3346565448832,21.2098942156211,-72.2289734905258));
#7076=CARTESIAN_POINT('Ctrl Pts',(-21.338294733384,21.2064553297857,-72.2292870003297));
#7077=CARTESIAN_POINT('Ctrl Pts',(-21.3440586288385,21.2010325591233,-72.2297815798355));
#7078=CARTESIAN_POINT('Ctrl Pts',(-21.3461790139652,21.19904306737,-72.2299630740623));
#7079=CARTESIAN_POINT('Ctrl Pts',(-21.3501927173132,21.1952873345385,-72.2303057747627));
#7080=CARTESIAN_POINT('Ctrl Pts',(-21.3520854754084,21.1935205020732,-72.230467026579));
#7081=CARTESIAN_POINT('Ctrl Pts',(-21.3553544641469,21.1904763641217,-72.2307449067749));
#7082=CARTESIAN_POINT('Ctrl Pts',(-21.3567296835061,21.1891979786376,-72.2308616189321));
#7083=CARTESIAN_POINT('Ctrl Pts',(-21.3593900727635,21.1867292470412,-72.2310870359558));
#7084=CARTESIAN_POINT('Ctrl Pts',(-21.3606750942658,21.1855387484659,-72.2311957528207));
#7085=CARTESIAN_POINT('Ctrl Pts',(-21.3637004504339,21.1827405101829,-72.2314513235572));
#7086=CARTESIAN_POINT('Ctrl Pts',(-21.3654415915475,21.1811336381043,-72.2315981103094));
#7087=CARTESIAN_POINT('Ctrl Pts',(-21.3705773720386,21.1764043828781,-72.2320302093342));
#7088=CARTESIAN_POINT('Ctrl Pts',(-21.3739769624592,21.1732873483914,-72.2323151130392));
#7089=CARTESIAN_POINT('Ctrl Pts',(-21.4031846320796,21.1466224535026,-72.2347533989894));
#7090=CARTESIAN_POINT('Ctrl Pts',(-21.4293686193564,21.1234872376781,-72.2368760140068));
#7091=CARTESIAN_POINT('Ctrl Pts',(-21.460783207273,21.0966273846338,-72.2393561618848));
#7092=CARTESIAN_POINT('Ctrl Pts',(-21.4656538627591,21.0924879354044,-72.2397388401132));
#7093=CARTESIAN_POINT('Ctrl Pts',(-21.4716997283573,21.0873806057529,-72.2402116079772));
#7094=CARTESIAN_POINT('Ctrl Pts',(-21.4728633140779,21.0863990623501,-72.2403024942067));
#7095=CARTESIAN_POINT('Ctrl Pts',(-21.4771658183141,21.0827748970356,-72.2406381805694));
#7096=CARTESIAN_POINT('Ctrl Pts',(-21.4803091007653,21.0801374348168,-72.2408826826033));
#7097=CARTESIAN_POINT('Ctrl Pts',(-21.4850460500589,21.0761781517422,-72.2412500514004));
#7098=CARTESIAN_POINT('Ctrl Pts',(-21.4866359559471,21.0748518615668,-72.2413731693396));
#7099=CARTESIAN_POINT('Ctrl Pts',(-21.6612455209653,20.9294787201626,-72.254874260667));
#7100=CARTESIAN_POINT('Ctrl Pts',(-21.8489032789655,20.8039388854537,-72.2672431215133));
#7101=CARTESIAN_POINT('Ctrl Pts',(-22.1509140677271,20.64483267797,-72.2863604295186));
#7102=CARTESIAN_POINT('Ctrl Pts',(-22.2565396898978,20.5962861569875,-72.2929097634569));
#7103=CARTESIAN_POINT('Ctrl Pts',(-22.4411712549438,20.5232331816516,-72.304371504602));
#7104=CARTESIAN_POINT('Ctrl Pts',(-22.5189215182431,20.4958684455546,-72.309201141605));
#7105=CARTESIAN_POINT('Ctrl Pts',(-22.6378260914721,20.4590770404931,-72.3166436325809));
#7106=CARTESIAN_POINT('Ctrl Pts',(-22.6782597576692,20.4474286125936,-72.3191838685214));
#7107=CARTESIAN_POINT('Ctrl Pts',(-22.7262265413084,20.4346216001707,-72.3222121398206));
#7108=CARTESIAN_POINT('Ctrl Pts',(-22.7335514206105,20.4326935141443,-72.3226749799785));
#7109=CARTESIAN_POINT('Ctrl Pts',(-22.7448012344292,20.4297746585994,-72.3233864643725));
#7110=CARTESIAN_POINT('Ctrl Pts',(-22.7487213865226,20.4287654226674,-72.3236345094717));
#7111=CARTESIAN_POINT('Ctrl Pts',(-22.7555678130577,20.4270165702933,-72.3240679234259));
#7112=CARTESIAN_POINT('Ctrl Pts',(-22.75849325071,20.4262736723706,-72.3242531857306));
#7113=CARTESIAN_POINT('Ctrl Pts',(-22.7650832510381,20.4246100313381,-72.3246706706643));
#7114=CARTESIAN_POINT('Ctrl Pts',(-22.7687483932925,20.4236916221987,-72.3249029685249));
#7115=CARTESIAN_POINT('Ctrl Pts',(-22.7785742756673,20.4212478156044,-72.3255260255025));
#7116=CARTESIAN_POINT('Ctrl Pts',(-22.7847378976524,20.4197341739326,-72.3259171640728));
#7117=CARTESIAN_POINT('Ctrl Pts',(-22.8114845180007,20.4132495422801,-72.3276158359357));
#7118=CARTESIAN_POINT('Ctrl Pts',(-22.8321113843946,20.4084633612162,-72.3289293178218));
#7119=CARTESIAN_POINT('Ctrl Pts',(-22.8656332182331,20.4010324399458,-72.3310699286203));
#7120=CARTESIAN_POINT('Ctrl Pts',(-22.8785000792891,20.3982627752031,-72.3318929958256));
#7121=CARTESIAN_POINT('Ctrl Pts',(-22.8973149140474,20.3943332127647,-72.3330986856588));
#7122=CARTESIAN_POINT('Ctrl Pts',(-22.9032498844473,20.3931111262805,-72.3334793201486));
#7123=CARTESIAN_POINT('Ctrl Pts',(-22.9175212831654,20.3902143942384,-72.3343953590149));
#7124=CARTESIAN_POINT('Ctrl Pts',(-22.9258609289715,20.3885559954558,-72.3349312740036));
#7125=CARTESIAN_POINT('Ctrl Pts',(-22.9357176618942,20.3866364321928,-72.3355654177624));
#7126=CARTESIAN_POINT('Ctrl Pts',(-22.9372285557843,20.3863433142591,-72.3356626432658));
#7127=CARTESIAN_POINT('Ctrl Pts',(-22.9504859006057,20.3837812025614,-72.3365159289196));
#7128=CARTESIAN_POINT('Ctrl Pts',(-22.9622445651909,20.3815765755326,-72.3372739951741));
#7129=CARTESIAN_POINT('Ctrl Pts',(-22.9779258405216,20.3787267916119,-72.3382866209504));
#7130=CARTESIAN_POINT('Ctrl Pts',(-22.981837871107,20.3780233257826,-72.338539380669));
#7131=CARTESIAN_POINT('Ctrl Pts',(-22.9906961328552,20.3764473351559,-72.3391120351599));
#7132=CARTESIAN_POINT('Ctrl Pts',(-22.9956431141157,20.37557913392,-72.3394320612992));
#7133=CARTESIAN_POINT('Ctrl Pts',(-23.0216604490222,20.3710757282314,-72.3411163231002));
#7134=CARTESIAN_POINT('Ctrl Pts',(-23.0427641804424,20.3676387824754,-72.3424865316952));
#7135=CARTESIAN_POINT('Ctrl Pts',(-23.3621365272321,20.3188832018215,-72.3632836424348));
#7136=CARTESIAN_POINT('Ctrl Pts',(-23.6652637311821,20.3154655364759,-72.3840330942772));
#7137=CARTESIAN_POINT('Ctrl Pts',(-24.0313702638923,20.3629009939869,-72.408712319235));
#7138=CARTESIAN_POINT('Ctrl Pts',(-24.0981007429276,20.3736903122922,-72.4131852351952));
#7139=CARTESIAN_POINT('Ctrl Pts',(-24.2133381993442,20.3960623864423,-72.4208138778078));
#7140=CARTESIAN_POINT('Ctrl Pts',(-24.2620068863861,20.4066869632356,-72.4240055181291));
#7141=CARTESIAN_POINT('Ctrl Pts',(-24.3162994703718,20.4198649608222,-72.4275172992848));
#7142=CARTESIAN_POINT('Ctrl Pts',(-24.3221820927456,20.4213103765406,-72.4278971559662));
#7143=CARTESIAN_POINT('Ctrl Pts',(-24.3312906976889,20.4235756977035,-72.4284842835377));
#7144=CARTESIAN_POINT('Ctrl Pts',(-24.3345195058716,20.4243840196792,-72.4286922051947));
#7145=CARTESIAN_POINT('Ctrl Pts',(-24.3398902796061,20.425737421379,-72.4290377163125));
#7146=CARTESIAN_POINT('Ctrl Pts',(-24.3420329374471,20.4262797026431,-72.4291754659622));
#7147=CARTESIAN_POINT('Ctrl Pts',(-24.3462001499589,20.4273389373883,-72.4294431927061));
#7148=CARTESIAN_POINT('Ctrl Pts',(-24.348224762364,20.4278556562696,-72.4295731833326));
#7149=CARTESIAN_POINT('Ctrl Pts',(-24.3520168662245,20.428827401178,-72.4298164993709));
#7150=CARTESIAN_POINT('Ctrl Pts',(-24.3537844616703,20.4292819565245,-72.4299298510646));
#7151=CARTESIAN_POINT('Ctrl Pts',(-24.3578025827445,20.4303188975417,-72.430187378812));
#7152=CARTESIAN_POINT('Ctrl Pts',(-24.36005286077,20.4309022157488,-72.4303314995742));
#7153=CARTESIAN_POINT('Ctrl Pts',(-24.365771246557,20.4323911434937,-72.4306974803245));
#7154=CARTESIAN_POINT('Ctrl Pts',(-24.369238488558,20.4333001077603,-72.4309191452699));
#7155=CARTESIAN_POINT('Ctrl Pts',(-24.3883551037096,20.4383457760665,-72.4321400000635));
#7156=CARTESIAN_POINT('Ctrl Pts',(-24.4039750222881,20.442594649655,-72.4331327595173));
#7157=CARTESIAN_POINT('Ctrl Pts',(-24.7094583233584,20.5281682197159,-72.4524664718376));
#7158=CARTESIAN_POINT('Ctrl Pts',(-24.9865995929362,20.6496098320321,-72.4686576850556));
#7159=CARTESIAN_POINT('Ctrl Pts',(-25.3126511677611,20.8508470818915,-72.4902690497409));
#7160=CARTESIAN_POINT('Ctrl Pts',(-25.380744556037,20.8965501001412,-72.4949353947562));
#7161=CARTESIAN_POINT('Ctrl Pts',(-25.5102313377665,20.9908162278489,-72.5042050018888));
#7162=CARTESIAN_POINT('Ctrl Pts',(-25.571744180153,21.0391170872353,-72.5087979869266));
#7163=CARTESIAN_POINT('Ctrl Pts',(-25.6617446867427,21.1152383374561,-72.5158548421325));
#7164=CARTESIAN_POINT('Ctrl Pts',(-25.6915754173723,21.1414293062824,-72.5182530021999));
#7165=CARTESIAN_POINT('Ctrl Pts',(-25.7264215175184,21.1731825639828,-72.5211288614429));
#7166=CARTESIAN_POINT('Ctrl Pts',(-25.7319117638342,21.1782204746584,-72.5215842186927));
#7167=CARTESIAN_POINT('Ctrl Pts',(-25.740338177641,21.1860066478047,-72.5222865901318));
#7168=CARTESIAN_POINT('Ctrl Pts',(-25.7432867804627,21.1887414646936,-72.5225330290847));
#7169=CARTESIAN_POINT('Ctrl Pts',(-25.748653055057,21.1937373802264,-72.5229827464392));
#7170=CARTESIAN_POINT('Ctrl Pts',(-25.7510723802493,21.195996701438,-72.5231859483396));
#7171=CARTESIAN_POINT('Ctrl Pts',(-25.755964726714,21.2005796203704,-72.523597780786));
#7172=CARTESIAN_POINT('Ctrl Pts',(-25.7584375671663,21.2029034041796,-72.5238064192189));
#7173=CARTESIAN_POINT('Ctrl Pts',(-25.7654985778125,21.2095598263624,-72.5244035412513));
#7174=CARTESIAN_POINT('Ctrl Pts',(-25.7700776796803,21.2139020235089,-72.5247924380626));
#7175=CARTESIAN_POINT('Ctrl Pts',(-25.7897424767466,21.2326594427524,-72.526469742548));
#7176=CARTESIAN_POINT('Ctrl Pts',(-25.8047004632204,21.2472072800857,-72.527763916228));
#7177=CARTESIAN_POINT('Ctrl Pts',(-26.0705967407166,21.5108853698052,-72.5511055858821));
#7178=CARTESIAN_POINT('Ctrl Pts',(-26.2789393451483,21.7994567368782,-72.5752273288794));
#7179=CARTESIAN_POINT('Ctrl Pts',(-26.465544546221,22.1749239035985,-72.6034019168748));
#7180=CARTESIAN_POINT('Ctrl Pts',(-26.4930465590552,22.234798044973,-72.6077960018667));
#7181=CARTESIAN_POINT('Ctrl Pts',(-26.5436492890504,22.3545096144307,-72.6163377765977));
#7182=CARTESIAN_POINT('Ctrl Pts',(-26.5668387211603,22.4142796741457,-72.6204870855576));
#7183=CARTESIAN_POINT('Ctrl Pts',(-26.5934400647382,22.4894175976518,-72.6255275210407));
#7184=CARTESIAN_POINT('Ctrl Pts',(-26.5985416333777,22.5041671170987,-72.6265086575913));
#7185=CARTESIAN_POINT('Ctrl Pts',(-26.6047295868064,22.5224872886051,-72.6277165468396));
#7186=CARTESIAN_POINT('Ctrl Pts',(-26.6059170677132,22.5260232025104,-72.6279491822946));
#7187=CARTESIAN_POINT('Ctrl Pts',(-26.6077782979381,22.5315973596767,-72.6283151295849));
#7188=CARTESIAN_POINT('Ctrl Pts',(-26.6084561493253,22.5336342139877,-72.6284486847928));
#7189=CARTESIAN_POINT('Ctrl Pts',(-26.6097197214898,22.5374437824164,-72.6286981639813));
#7190=CARTESIAN_POINT('Ctrl Pts',(-26.6103059330636,22.5392163162974,-72.6288141165264));
#7191=CARTESIAN_POINT('Ctrl Pts',(-26.6116190286327,22.5431983404738,-72.62907432295));
#7192=CARTESIAN_POINT('Ctrl Pts',(-26.6123450595428,22.545408104124,-72.6292185254383));
#7193=CARTESIAN_POINT('Ctrl Pts',(-26.6141852146144,22.5510293551839,-72.6295848599222));
#7194=CARTESIAN_POINT('Ctrl Pts',(-26.6152960371554,22.5544419313,-72.6298067962042));
#7195=CARTESIAN_POINT('Ctrl Pts',(-26.6214029148697,22.5733099958477,-72.6310313746163));
#7196=CARTESIAN_POINT('Ctrl Pts',(-26.626287887589,22.588801591821,-72.6320275402137));
#7197=CARTESIAN_POINT('Ctrl Pts',(-26.7248916703118,22.9099471182035,-72.6524998026793));
#7198=CARTESIAN_POINT('Ctrl Pts',(-26.7727489747728,23.2278829040988,-72.6695650113928));
#7199=CARTESIAN_POINT('Ctrl Pts',(-26.7731395527062,23.7224995396896,-72.6975928801036));
#7200=CARTESIAN_POINT('Ctrl Pts',(-26.7590578347791,23.8969868809995,-72.7077368667361));
#7201=CARTESIAN_POINT('Ctrl Pts',(-26.7290519982083,24.0808028784832,-72.7190629401086));
#7202=CARTESIAN_POINT('Ctrl Pts',(-26.7271392598985,24.0921385248448,-72.7197639288064));
#7203=CARTESIAN_POINT('Ctrl Pts',(-26.7244033267836,24.1078402190251,-72.7207384940478));
#7204=CARTESIAN_POINT('Ctrl Pts',(-26.7236316758482,24.1122152583552,-72.7210104281687));
#7205=CARTESIAN_POINT('Ctrl Pts',(-26.7222893111018,24.1197351463267,-72.7214785023811));
#7206=CARTESIAN_POINT('Ctrl Pts',(-26.721722959129,24.1228807759146,-72.7216745031935));
#7207=CARTESIAN_POINT('Ctrl Pts',(-26.7205465398087,24.1293595569638,-72.7220786067355));
#7208=CARTESIAN_POINT('Ctrl Pts',(-26.7199358935016,24.1326925975788,-72.7222867276887));
#7209=CARTESIAN_POINT('Ctrl Pts',(-26.7185060201455,24.1404283106931,-72.7227702913915));
#7210=CARTESIAN_POINT('Ctrl Pts',(-26.7176828721995,24.1448302431195,-72.7230458590531));
#7211=CARTESIAN_POINT('Ctrl Pts',(-26.715045990241,24.1587705658784,-72.7239198220993));
#7212=CARTESIAN_POINT('Ctrl Pts',(-26.7131983376488,24.1683024151757,-72.724519300635));
#7213=CARTESIAN_POINT('Ctrl Pts',(-26.681546985842,24.3277287179517,-72.7345781686208));
#7214=CARTESIAN_POINT('Ctrl Pts',(-26.6411660145329,24.4753014730892,-72.7443807014553));
#7215=CARTESIAN_POINT('Ctrl Pts',(-26.5342127841754,24.7794231094666,-72.7656486709851));
#7216=CARTESIAN_POINT('Ctrl Pts',(-26.465411370887,24.9347090509299,-72.7771487632234));
#7217=CARTESIAN_POINT('Ctrl Pts',(-26.3269578320015,25.1906058697027,-72.7968275056138));
#7218=CARTESIAN_POINT('Ctrl Pts',(-26.2632064498773,25.2940232689196,-72.8050005531721));
#7219=CARTESIAN_POINT('Ctrl Pts',(-26.1850678330646,25.4060804532983,-72.8139364889437));
#7220=CARTESIAN_POINT('Ctrl Pts',(-26.1762788674388,25.418496264952,-72.8149276800251));
#7221=CARTESIAN_POINT('Ctrl Pts',(-26.1648304170246,25.4344286028968,-72.8162005712717));
#7222=CARTESIAN_POINT('Ctrl Pts',(-26.1622513064208,25.4380023527754,-72.8164861539765));
#7223=CARTESIAN_POINT('Ctrl Pts',(-26.1590290828877,25.4424479872635,-72.8168414777987));
#7224=CARTESIAN_POINT('Ctrl Pts',(-26.1583928633286,25.4433248352904,-72.8169115644473));
#7225=CARTESIAN_POINT('Ctrl Pts',(-26.1558068923294,25.4468850839916,-72.8171961487189));
#7226=CARTESIAN_POINT('Ctrl Pts',(-26.1538534335845,25.4495658045689,-72.8174104585923));
#7227=CARTESIAN_POINT('Ctrl Pts',(-26.1511454710819,25.4532698981009,-72.8177066177129));
#7228=CARTESIAN_POINT('Ctrl Pts',(-26.1503945020535,25.4542958381839,-72.8177886500965));
#7229=CARTESIAN_POINT('Ctrl Pts',(-26.1481278891553,25.4573885410731,-72.8180359480855));
#7230=CARTESIAN_POINT('Ctrl Pts',(-26.1466103830061,25.4594539456866,-72.8182011161122));
#7231=CARTESIAN_POINT('Ctrl Pts',(-26.1217003066156,25.4932732273269,-72.8209058162147));
#7232=CARTESIAN_POINT('Ctrl Pts',(-26.0977278818961,25.5245986956891,-72.8234141521142));
#7233=CARTESIAN_POINT('Ctrl Pts',(-26.070213032434,25.5592173033174,-72.8261823247367));
#7234=CARTESIAN_POINT('Ctrl Pts',(-26.0672326213908,25.5629501263868,-72.8264807571691));
#7235=CARTESIAN_POINT('Ctrl Pts',(-26.062735144519,25.5685573891051,-72.8269289520568));
#7236=CARTESIAN_POINT('Ctrl Pts',(-26.061224272843,25.570436754096,-72.8270791556201));
#7237=CARTESIAN_POINT('Ctrl Pts',(-26.0586054522387,25.5736868139997,-72.8273388777985));
#7238=CARTESIAN_POINT('Ctrl Pts',(-26.0574984884602,25.5750582954968,-72.8274484675571));
#7239=CARTESIAN_POINT('Ctrl Pts',(-26.0551912572214,25.5779120646658,-72.8276764801144));
#7240=CARTESIAN_POINT('Ctrl Pts',(-26.053990800291,25.5793941932541,-72.8277948882979));
#7241=CARTESIAN_POINT('Ctrl Pts',(-26.0511377967888,25.5829102306204,-72.8280757603484));
#7242=CARTESIAN_POINT('Ctrl Pts',(-26.0494840789561,25.5849431969942,-72.8282381391084));
#7243=CARTESIAN_POINT('Ctrl Pts',(-26.0439678112563,25.5917076433767,-72.8287783733276));
#7244=CARTESIAN_POINT('Ctrl Pts',(-26.0400942600907,25.5964301968834,-72.829155434366));
#7245=CARTESIAN_POINT('Ctrl Pts',(-26.0309136877108,25.6075582905587,-72.8300437715298));
#7246=CARTESIAN_POINT('Ctrl Pts',(-26.0255952164739,25.6139543882733,-72.8305542362187));
#7247=CARTESIAN_POINT('Ctrl Pts',(-25.830583953334,25.8466402374352,-72.8491230536153));
#7248=CARTESIAN_POINT('Ctrl Pts',(-25.6106763437511,26.045854643975,-72.8650564241307));
#7249=CARTESIAN_POINT('Ctrl Pts',(-25.2001645860434,26.325957729553,-72.8930255219344));
#7250=CARTESIAN_POINT('Ctrl Pts',(-25.023395032122,26.4236793804682,-72.9046130661058));
#7251=CARTESIAN_POINT('Ctrl Pts',(-24.8267094650557,26.5094662182072,-72.9176484156279));
#7252=CARTESIAN_POINT('Ctrl Pts',(-24.8147134749497,26.5146118992978,-72.9184438163855));
#7253=CARTESIAN_POINT('Ctrl Pts',(-24.7983664890463,26.5215066602354,-72.919528318545));
#7254=CARTESIAN_POINT('Ctrl Pts',(-24.7940423326493,26.5233193788359,-72.9198152518033));
#7255=CARTESIAN_POINT('Ctrl Pts',(-24.786702069711,26.5263776551955,-72.9203024245227));
#7256=CARTESIAN_POINT('Ctrl Pts',(-24.7836879896329,26.5276280843882,-72.9205024981912));
#7257=CARTESIAN_POINT('Ctrl Pts',(-24.7776263806347,26.5301320353331,-72.9209049271581));
#7258=CARTESIAN_POINT('Ctrl Pts',(-24.7745788186264,26.5313854647032,-72.9211072852558));
#7259=CARTESIAN_POINT('Ctrl Pts',(-24.7676763270436,26.5342120153748,-72.9215656835205));
#7260=CARTESIAN_POINT('Ctrl Pts',(-24.7638202662534,26.5357823424828,-72.9218218180042));
#7261=CARTESIAN_POINT('Ctrl Pts',(-24.7557591654865,26.5390469159325,-72.9223573792923));
#7262=CARTESIAN_POINT('Ctrl Pts',(-24.7515535745491,26.5407397694985,-72.9226368526282));
#7263=CARTESIAN_POINT('Ctrl Pts',(-24.740556617399,26.5451393735151,-72.9233678038495));
#7264=CARTESIAN_POINT('Ctrl Pts',(-24.7337596163371,26.5478318869312,-72.9238197619237));
#7265=CARTESIAN_POINT('Ctrl Pts',(-24.713632318278,26.5557258366114,-72.9251586394627));
#7266=CARTESIAN_POINT('Ctrl Pts',(-24.7002766079937,26.560861594273,-72.9260477646332));
#7267=CARTESIAN_POINT('Ctrl Pts',(-24.5575115091148,26.614671377569,-72.9355601647306));
#7268=CARTESIAN_POINT('Ctrl Pts',(-24.4251497914064,26.6550519062576,-72.9444602045012));
#7269=CARTESIAN_POINT('Ctrl Pts',(-24.1249901353173,26.7259029852119,-72.9648141469786));
#7270=CARTESIAN_POINT('Ctrl Pts',(-23.9565347422769,26.7518155470262,-72.9763578071717));
#7271=CARTESIAN_POINT('Ctrl Pts',(-23.6452405225055,26.7747296978135,-72.9974666016246));
#7272=CARTESIAN_POINT('Ctrl Pts',(-23.5030969908233,26.7757849281901,-73.0070146660093));
#7273=CARTESIAN_POINT('Ctrl Pts',(-23.3529920376228,26.7669706931905,-73.01672966143));
#7274=CARTESIAN_POINT('Ctrl Pts',(-23.3446494008634,26.7664482329231,-73.0172683770659));
#7275=CARTESIAN_POINT('Ctrl Pts',(-23.2996452972319,26.763454009875,-73.0201674894931));
#7276=CARTESIAN_POINT('Ctrl Pts',(-23.2630242042034,26.7603877158433,-73.0225016189072));
#7277=CARTESIAN_POINT('Ctrl Pts',(-23.2213547699675,26.7561798813537,-73.0251229710299));
#7278=CARTESIAN_POINT('Ctrl Pts',(-23.2162490586078,26.7556519747898,-73.025443569872));
#7279=CARTESIAN_POINT('Ctrl Pts',(-23.2087075992699,26.7548540087959,-73.0259162170039));
#7280=CARTESIAN_POINT('Ctrl Pts',(-23.2062708953098,26.7545933690325,-73.0260687944292));
#7281=CARTESIAN_POINT('Ctrl Pts',(-23.2019590315102,26.7541271794695,-73.0263385394056));
#7282=CARTESIAN_POINT('Ctrl Pts',(-23.2000837538161,26.7539227625389,-73.0264557713762));
#7283=CARTESIAN_POINT('Ctrl Pts',(-23.1961694684679,26.7534926031359,-73.0267002962069));
#7284=CARTESIAN_POINT('Ctrl Pts',(-23.1941305010251,26.7532665607428,-73.0268275715536));
#7285=CARTESIAN_POINT('Ctrl Pts',(-23.188808818646,26.7526714482595,-73.0271595045077));
#7286=CARTESIAN_POINT('Ctrl Pts',(-23.1855264422285,26.7522992763207,-73.0273639858034));
#7287=CARTESIAN_POINT('Ctrl Pts',(-23.1712915703238,26.7506630845301,-73.0282496982272));
#7288=CARTESIAN_POINT('Ctrl Pts',(-23.1603448593197,26.7493478932452,-73.0289280598057));
#7289=CARTESIAN_POINT('Ctrl Pts',(-23.0812273695827,26.7394301966803,-73.033812370134));
#7290=CARTESIAN_POINT('Ctrl Pts',(-23.0133346995317,26.7287049257098,-73.0379040780433));
#7291=CARTESIAN_POINT('Ctrl Pts',(-22.8852406234207,26.7042471113173,-73.0455220153909));
#7292=CARTESIAN_POINT('Ctrl Pts',(-22.8249915555888,26.6909403349312,-73.0490616380125));
#7293=CARTESIAN_POINT('Ctrl Pts',(-22.5255467966103,26.6157267111193,-73.0665963264064));
#7294=CARTESIAN_POINT('Ctrl Pts',(-22.2940244688461,26.5282848930883,-73.0800376425379));
#7295=CARTESIAN_POINT('Ctrl Pts',(-22.0750359288982,26.4155367300479,-73.0942273918944));
#7296=CARTESIAN_POINT('Ctrl Pts',(-22.0750360358082,26.4155367850914,-73.3444460357026));
#7297=CARTESIAN_POINT('Ctrl Pts',(-22.0900522043839,26.4232679899663,-73.3434851462927));
#7298=CARTESIAN_POINT('Ctrl Pts',(-22.105130934277,26.4308820708058,-73.3425217028701));
#7299=CARTESIAN_POINT('Ctrl Pts',(-22.2119811348726,26.4837862176688,-73.3357019430998));
#7300=CARTESIAN_POINT('Ctrl Pts',(-22.3057946946976,26.5247965351268,-73.3297496648075));
#7301=CARTESIAN_POINT('Ctrl Pts',(-22.4457726315562,26.5782052841756,-73.3208151658341));
#7302=CARTESIAN_POINT('Ctrl Pts',(-22.4905180480599,26.5941540051938,-73.3179519354376));
#7303=CARTESIAN_POINT('Ctrl Pts',(-22.5430287315366,26.6115723569861,-73.3145780437848));
#7304=CARTESIAN_POINT('Ctrl Pts',(-22.5504685232802,26.6140101577384,-73.3140997105509));
#7305=CARTESIAN_POINT('Ctrl Pts',(-22.5618211435582,26.6176843225716,-73.3133693009795));
#7306=CARTESIAN_POINT('Ctrl Pts',(-22.5657276096154,26.618940374779,-73.3131178741964));
#7307=CARTESIAN_POINT('Ctrl Pts',(-22.572824967011,26.6212074519544,-73.312660907058));
#7308=CARTESIAN_POINT('Ctrl Pts',(-22.5760150595697,26.622220974606,-73.3124554492909));
#7309=CARTESIAN_POINT('Ctrl Pts',(-22.5824059855557,26.6242404762025,-73.3120437156098));
#7310=CARTESIAN_POINT('Ctrl Pts',(-22.5856068224958,26.6252464301344,-73.3118374391682));
#7311=CARTESIAN_POINT('Ctrl Pts',(-22.5946462553478,26.6280718257314,-73.3112547150411));
#7312=CARTESIAN_POINT('Ctrl Pts',(-22.6004884445562,26.6298796422545,-73.3108778859467));
#7313=CARTESIAN_POINT('Ctrl Pts',(-22.6247430722789,26.6373094518428,-73.3093125141375));
#7314=CARTESIAN_POINT('Ctrl Pts',(-22.643200257472,26.6427829411889,-73.3081191152857));
#7315=CARTESIAN_POINT('Ctrl Pts',(-23.0385023733989,26.7561667540438,-73.2825093410385));
#7316=CARTESIAN_POINT('Ctrl Pts',(-23.4318113181324,26.7945645748825,-73.255453978345));
#7317=CARTESIAN_POINT('Ctrl Pts',(-23.9262068513738,26.7527011995316,-73.2224555356987));
#7318=CARTESIAN_POINT('Ctrl Pts',(-24.0297685483208,26.7388397901194,-73.2156390797172));
#7319=CARTESIAN_POINT('Ctrl Pts',(-24.1370323364614,26.7191369402607,-73.2088003734989));
#7320=CARTESIAN_POINT('Ctrl Pts',(-24.1415774437726,26.7182919542899,-73.2085110176226));
#7321=CARTESIAN_POINT('Ctrl Pts',(-24.1488246606203,26.7169284764174,-73.2080503272773));
#7322=CARTESIAN_POINT('Ctrl Pts',(-24.1515279303664,26.7164163031219,-73.2078786394513));
#7323=CARTESIAN_POINT('Ctrl Pts',(-24.156662885971,26.7154365984318,-73.2075528081832));
#7324=CARTESIAN_POINT('Ctrl Pts',(-24.1590946932532,26.714969725459,-73.207398627449));
#7325=CARTESIAN_POINT('Ctrl Pts',(-24.1633511314254,26.7141474612139,-73.2071289857693));
#7326=CARTESIAN_POINT('Ctrl Pts',(-24.1651759952896,26.7137932935657,-73.2070134543003));
#7327=CARTESIAN_POINT('Ctrl Pts',(-24.1687486937133,26.7130966998768,-73.2067874104048));
#7328=CARTESIAN_POINT('Ctrl Pts',(-24.1704965472834,26.7127544045479,-73.2066768906468));
#7329=CARTESIAN_POINT('Ctrl Pts',(-24.1746782486419,26.711931870389,-73.2064126319414));
#7330=CARTESIAN_POINT('Ctrl Pts',(-24.1771118319032,26.7114502690326,-73.2062589715544));
#7331=CARTESIAN_POINT('Ctrl Pts',(-24.1858496587277,26.7097105834375,-73.2057077016014));
#7332=CARTESIAN_POINT('Ctrl Pts',(-24.192150745365,26.7084364360284,-73.2053110083888));
#7333=CARTESIAN_POINT('Ctrl Pts',(-24.2874983246582,26.6888589863246,-73.199320463505));
#7334=CARTESIAN_POINT('Ctrl Pts',(-24.3757449828602,26.6668127564783,-73.193936865044));
#7335=CARTESIAN_POINT('Ctrl Pts',(-24.7480232203334,26.5568811999074,-73.1714616144944));
#7336=CARTESIAN_POINT('Ctrl Pts',(-25.0200897020776,26.4336665388322,-73.1555022266506));
#7337=CARTESIAN_POINT('Ctrl Pts',(-25.3411740531659,26.2308351628172,-73.1335811151271));
#7338=CARTESIAN_POINT('Ctrl Pts',(-25.4091972318549,26.1841177744388,-73.128746296913));
#7339=CARTESIAN_POINT('Ctrl Pts',(-25.5092059264325,26.1096277126221,-73.121290228028));
#7340=CARTESIAN_POINT('Ctrl Pts',(-25.5425620816965,26.0837485586612,-73.1187416376436));
#7341=CARTESIAN_POINT('Ctrl Pts',(-25.5812970548647,26.0524581971578,-73.1157043845115));
#7342=CARTESIAN_POINT('Ctrl Pts',(-25.5871781094714,26.0476730482326,-73.1152410885986));
#7343=CARTESIAN_POINT('Ctrl Pts',(-25.596174479669,26.040300191122,-73.1145290354615));
#7344=CARTESIAN_POINT('Ctrl Pts',(-25.5993019222952,26.0377272668554,-73.1142808787871));
#7345=CARTESIAN_POINT('Ctrl Pts',(-25.6047520678864,26.0332262188089,-73.1138473272955));
#7346=CARTESIAN_POINT('Ctrl Pts',(-25.6070769319805,26.0313007096638,-73.1136620392027));
#7347=CARTESIAN_POINT('Ctrl Pts',(-25.6119367962838,26.0272641260413,-73.1132739836985));
#7348=CARTESIAN_POINT('Ctrl Pts',(-25.6144712660578,26.0251524209749,-73.1130711906292));
#7349=CARTESIAN_POINT('Ctrl Pts',(-25.6214840800703,26.0192911200139,-73.1125089044615));
#7350=CARTESIAN_POINT('Ctrl Pts',(-25.6259554635248,26.0155332491118,-73.1121490722885));
#7351=CARTESIAN_POINT('Ctrl Pts',(-25.6435475854368,26.0006665661759,-73.1107281257167));
#7352=CARTESIAN_POINT('Ctrl Pts',(-25.6565893741395,25.9894651526301,-73.1096631985598));
#7353=CARTESIAN_POINT('Ctrl Pts',(-25.8717529929242,25.8016516950782,-73.0918991879337));
#7354=CARTESIAN_POINT('Ctrl Pts',(-26.0510773937628,25.600612391256,-73.0740793885299));
#7355=CARTESIAN_POINT('Ctrl Pts',(-26.283884961126,25.2629932991459,-73.0463324259503));
#7356=CARTESIAN_POINT('Ctrl Pts',(-26.3565963822766,25.141058819488,-73.0367027737387));
#7357=CARTESIAN_POINT('Ctrl Pts',(-26.4500821039092,24.9578000628833,-73.0231016822347));
#7358=CARTESIAN_POINT('Ctrl Pts',(-26.4774248028125,24.9000174275619,-73.0189323365691));
#7359=CARTESIAN_POINT('Ctrl Pts',(-26.5142904813043,24.8157113866528,-73.0130563135091));
#7360=CARTESIAN_POINT('Ctrl Pts',(-26.5252114700685,24.7898196043361,-73.0112791636726));
#7361=CARTESIAN_POINT('Ctrl Pts',(-26.5374619143955,24.759681038465,-73.0092449280717));
#7362=CARTESIAN_POINT('Ctrl Pts',(-26.5391225025742,24.7555713720106,-73.0089682771066));
#7363=CARTESIAN_POINT('Ctrl Pts',(-26.5416313662326,24.7493253044259,-73.008548940211));
#7364=CARTESIAN_POINT('Ctrl Pts',(-26.5424858348326,24.7471914214038,-73.0084058795575));
#7365=CARTESIAN_POINT('Ctrl Pts',(-26.5440294629696,24.7433245021043,-73.0081469965661));
#7366=CARTESIAN_POINT('Ctrl Pts',(-26.5447193990714,24.7415917869236,-73.0080311271481));
#7367=CARTESIAN_POINT('Ctrl Pts',(-26.5462077605569,24.7378444335398,-73.0077808224934));
#7368=CARTESIAN_POINT('Ctrl Pts',(-26.5470056559175,24.7358295942267,-73.0076464199407));
#7369=CARTESIAN_POINT('Ctrl Pts',(-26.549168832447,24.7303510212098,-73.0072814460406));
#7370=CARTESIAN_POINT('Ctrl Pts',(-26.5505301500167,24.7268857103878,-73.0070511153188));
#7371=CARTESIAN_POINT('Ctrl Pts',(-26.5569608695626,24.7104322264947,-73.0059599363398));
#7372=CARTESIAN_POINT('Ctrl Pts',(-26.5619520570333,24.6974133482053,-73.0051037548949));
#7373=CARTESIAN_POINT('Ctrl Pts',(-26.6498501318137,24.4636142018348,-72.9898500352905));
#7374=CARTESIAN_POINT('Ctrl Pts',(-26.7083752173632,24.2343830622935,-72.97680646124));
#7375=CARTESIAN_POINT('Ctrl Pts',(-26.7623425028029,23.8521346975943,-72.9552321719404));
#7376=CARTESIAN_POINT('Ctrl Pts',(-26.7729160826212,23.7022071080646,-72.9468182263386));
#7377=CARTESIAN_POINT('Ctrl Pts',(-26.7730250382214,23.5118544729735,-72.935799676369));
#7378=CARTESIAN_POINT('Ctrl Pts',(-26.7722943008018,23.471616057052,-72.9334522222895));
#7379=CARTESIAN_POINT('Ctrl Pts',(-26.7703932184515,23.4201009692817,-72.9304180254313));
#7380=CARTESIAN_POINT('Ctrl Pts',(-26.7699166489407,23.4088013408913,-72.9297507095289));
#7381=CARTESIAN_POINT('Ctrl Pts',(-26.7688945832923,23.3872615454365,-72.9284750969429));
#7382=CARTESIAN_POINT('Ctrl Pts',(-26.7683596696402,23.3770210010631,-72.9278671090946));
#7383=CARTESIAN_POINT('Ctrl Pts',(-26.7647325812258,23.3134122996492,-72.9240807407934));
#7384=CARTESIAN_POINT('Ctrl Pts',(-26.7603619505714,23.2601279246421,-72.9208655149557));
#7385=CARTESIAN_POINT('Ctrl Pts',(-26.7537355380331,23.1982711537277,-72.9170744378423));
#7386=CARTESIAN_POINT('Ctrl Pts',(-26.7527672054969,23.1895670398442,-72.9165396310103));
#7387=CARTESIAN_POINT('Ctrl Pts',(-26.7512713702169,23.1766024455635,-72.9157410009461));
#7388=CARTESIAN_POINT('Ctrl Pts',(-26.750770808147,23.1723388467725,-72.915478029505));
#7389=CARTESIAN_POINT('Ctrl Pts',(-26.7498629422377,23.1647371728677,-72.9150085778163));
#7390=CARTESIAN_POINT('Ctrl Pts',(-26.7494589289791,23.1613987049362,-72.914802201925));
#7391=CARTESIAN_POINT('Ctrl Pts',(-26.7485962681694,23.1543626627979,-72.9143668178403));
#7392=CARTESIAN_POINT('Ctrl Pts',(-26.7481364324005,23.1506652416534,-72.9141377723295));
#7393=CARTESIAN_POINT('Ctrl Pts',(-26.7469052161776,23.1409036008926,-72.9135323936546));
#7394=CARTESIAN_POINT('Ctrl Pts',(-26.7461229941646,23.1348407857749,-72.9131557177424));
#7395=CARTESIAN_POINT('Ctrl Pts',(-26.7425094066653,23.1074471241554,-72.9114506578144));
#7396=CARTESIAN_POINT('Ctrl Pts',(-26.7394817509966,23.0861431315339,-72.9101160685041));
#7397=CARTESIAN_POINT('Ctrl Pts',(-26.7157546167207,22.9304008043411,-72.9002949672586));
#7398=CARTESIAN_POINT('Ctrl Pts',(-26.6867783771639,22.7973803545223,-72.8915445695326));
#7399=CARTESIAN_POINT('Ctrl Pts',(-26.6031703685121,22.5041409558594,-72.8714366189131));
#7400=CARTESIAN_POINT('Ctrl Pts',(-26.5441501841638,22.3455843788541,-72.8599851009913));
#7401=CARTESIAN_POINT('Ctrl Pts',(-26.3960421518399,22.0267875348199,-72.8362061523148));
#7402=CARTESIAN_POINT('Ctrl Pts',(-26.3051547035346,21.867993464027,-72.8239266993623));
#7403=CARTESIAN_POINT('Ctrl Pts',(-26.1949148444702,21.708512975136,-72.8117122868386));
#7404=CARTESIAN_POINT('Ctrl Pts',(-26.1884894621204,21.6993205365675,-72.8110087580274));
#7405=CARTESIAN_POINT('Ctrl Pts',(-26.1800165286662,21.6873325428035,-72.8100921451008));
#7406=CARTESIAN_POINT('Ctrl Pts',(-26.1780123739787,21.6845066282215,-72.8098761367108));
#7407=CARTESIAN_POINT('Ctrl Pts',(-26.1749142960959,21.6801531452956,-72.8095434686959));
#7408=CARTESIAN_POINT('Ctrl Pts',(-26.1738235953142,21.6786233038024,-72.8094265871414));
#7409=CARTESIAN_POINT('Ctrl Pts',(-26.1717556176469,21.6757280714165,-72.8092054276933));
#7410=CARTESIAN_POINT('Ctrl Pts',(-26.1707786167294,21.6743624977332,-72.809101131805));
#7411=CARTESIAN_POINT('Ctrl Pts',(-26.168504920955,21.671189750448,-72.8088588514499));
#7412=CARTESIAN_POINT('Ctrl Pts',(-26.1672074242551,21.6693831582107,-72.808720923714));
#7413=CARTESIAN_POINT('Ctrl Pts',(-26.1635229311059,21.6642641829456,-72.8083301835227));
#7414=CARTESIAN_POINT('Ctrl Pts',(-26.1611314980298,21.6609549755531,-72.8080776784895));
#7415=CARTESIAN_POINT('Ctrl Pts',(-26.1464963408314,21.6407840530583,-72.8065390661557));
#7416=CARTESIAN_POINT('Ctrl Pts',(-26.1340952357037,21.6240363645369,-72.8052637331039));
#7417=CARTESIAN_POINT('Ctrl Pts',(-26.0963887803696,21.574133286754,-72.8014662382974));
#7418=CARTESIAN_POINT('Ctrl Pts',(-26.0706004658224,21.5413464313524,-72.7989747481181));
#7419=CARTESIAN_POINT('Ctrl Pts',(-25.9944692493683,21.4483289544368,-72.7918866132314));
#7420=CARTESIAN_POINT('Ctrl Pts',(-25.9425512445703,21.3894224752071,-72.7873729420552));
#7421=CARTESIAN_POINT('Ctrl Pts',(-25.6421681319233,21.0727194466117,-72.7625919586977));
#7422=CARTESIAN_POINT('Ctrl Pts',(-25.3542774843463,20.8558546232499,-72.7433036193204));
#7423=CARTESIAN_POINT('Ctrl Pts',(-25.0184855840522,20.6813107291108,-72.7204177764769));
#7424=CARTESIAN_POINT('Ctrl Pts',(-25.0002602872651,20.6720564227562,-72.7191757507835));
#7425=CARTESIAN_POINT('Ctrl Pts',(-24.9763398392287,20.6601951368106,-72.7175453324585));
#7426=CARTESIAN_POINT('Ctrl Pts',(-24.970723106729,20.6574303631158,-72.7171624764299));
#7427=CARTESIAN_POINT('Ctrl Pts',(-24.9620583666122,20.6531965613691,-72.7165718148272));
#7428=CARTESIAN_POINT('Ctrl Pts',(-24.9590160198947,20.651715927668,-72.7163644147822));
#7429=CARTESIAN_POINT('Ctrl Pts',(-24.9529628700499,20.6487817931211,-72.7159517464647));
#7430=CARTESIAN_POINT('Ctrl Pts',(-24.9499521254376,20.6473281807566,-72.7157464824022));
#7431=CARTESIAN_POINT('Ctrl Pts',(-24.943360791487,20.6441584684106,-72.7152970813501));
#7432=CARTESIAN_POINT('Ctrl Pts',(-24.9397792854021,20.6424442971884,-72.7150528776313));
#7433=CARTESIAN_POINT('Ctrl Pts',(-24.929588500293,20.637589936801,-72.7143579759328));
#7434=CARTESIAN_POINT('Ctrl Pts',(-24.9229717131273,20.6344656475974,-72.7139067266474));
#7435=CARTESIAN_POINT('Ctrl Pts',(-24.9081169012327,20.6275133310221,-72.7128935136403));
#7436=CARTESIAN_POINT('Ctrl Pts',(-24.8998732408845,20.6236975570161,-72.712331129337));
#7437=CARTESIAN_POINT('Ctrl Pts',(-24.7231750070766,20.5428139480183,-72.7002741219425));
#7438=CARTESIAN_POINT('Ctrl Pts',(-24.5484334814491,20.4803914420529,-72.6882686001742));
#7439=CARTESIAN_POINT('Ctrl Pts',(-24.0945479515876,20.3611183529609,-72.6569649847195));
#7440=CARTESIAN_POINT('Ctrl Pts',(-23.8114407566507,20.3255644331804,-72.6372603477567));
#7441=CARTESIAN_POINT('Ctrl Pts',(-23.4904908376253,20.3278459271695,-72.6166287440313));
#7442=CARTESIAN_POINT('Ctrl Pts',(-23.4536429016258,20.3287400524288,-72.6142875485335));
#7443=CARTESIAN_POINT('Ctrl Pts',(-23.4116830737946,20.330478864922,-72.6116590157396));
#7444=CARTESIAN_POINT('Ctrl Pts',(-23.406550113058,20.3307038714546,-72.6113381058583));
#7445=CARTESIAN_POINT('Ctrl Pts',(-23.3989684754661,20.331054384918,-72.6108650727259));
#7446=CARTESIAN_POINT('Ctrl Pts',(-23.396519400924,20.3311704112015,-72.6107124192313));
#7447=CARTESIAN_POINT('Ctrl Pts',(-23.3921859554331,20.3313806672587,-72.6104425774347));
#7448=CARTESIAN_POINT('Ctrl Pts',(-23.3903015334821,20.3314737569987,-72.6103253245714));
#7449=CARTESIAN_POINT('Ctrl Pts',(-23.3863687875621,20.3316714953625,-72.6100808079457));
#7450=CARTESIAN_POINT('Ctrl Pts',(-23.3843204856661,20.3317764442916,-72.6099535616029));
#7451=CARTESIAN_POINT('Ctrl Pts',(-23.3789752638601,20.332055433948,-72.6096217742592));
#7452=CARTESIAN_POINT('Ctrl Pts',(-23.3756784980491,20.3322325862265,-72.6094174093098));
#7453=CARTESIAN_POINT('Ctrl Pts',(-23.3613899987229,20.333022403269,-72.6085328248107));
#7454=CARTESIAN_POINT('Ctrl Pts',(-23.350401002179,20.3336863299739,-72.6078554660607));
#7455=CARTESIAN_POINT('Ctrl Pts',(-23.2710178075202,20.3388908461009,-72.6029822961744));
#7456=CARTESIAN_POINT('Ctrl Pts',(-23.2027747722018,20.3455564928959,-72.5989001860272));
#7457=CARTESIAN_POINT('Ctrl Pts',(-23.0641761347029,20.3635743242518,-72.5907348462318));
#7458=CARTESIAN_POINT('Ctrl Pts',(-22.9938813217755,20.3750926306353,-72.586659912837));
#7459=CARTESIAN_POINT('Ctrl Pts',(-22.581214509676,20.4568383043441,-72.5628405632533));
#7460=CARTESIAN_POINT('Ctrl Pts',(-22.2517685331347,20.5800363411628,-72.543940432377));
#7461=CARTESIAN_POINT('Ctrl Pts',(-21.9306618056225,20.7639526614434,-72.5215643892726));
#7462=CARTESIAN_POINT('Ctrl Pts',(-21.9129025614361,20.7743515732138,-72.520313947));
#7463=CARTESIAN_POINT('Ctrl Pts',(-21.8898585775834,20.7881430340005,-72.5186740322847));
#7464=CARTESIAN_POINT('Ctrl Pts',(-21.8844821688591,20.7913821002464,-72.5182901776504));
#7465=CARTESIAN_POINT('Ctrl Pts',(-21.8762195282964,20.7963929609402,-72.5176983243276));
#7466=CARTESIAN_POINT('Ctrl Pts',(-21.8733265485137,20.7981536456268,-72.5174907338923));
#7467=CARTESIAN_POINT('Ctrl Pts',(-21.8676108914869,20.8016445868501,-72.5170798703797));
#7468=CARTESIAN_POINT('Ctrl Pts',(-21.8647880942096,20.8033746396749,-72.5168766049774));
#7469=CARTESIAN_POINT('Ctrl Pts',(-21.8586028039712,20.8071786411742,-72.5164304366106));
#7470=CARTESIAN_POINT('Ctrl Pts',(-21.855241452156,20.8092544269559,-72.5161874660522));
#7471=CARTESIAN_POINT('Ctrl Pts',(-21.8457395687584,20.8151464292877,-72.5154992039024));
#7472=CARTESIAN_POINT('Ctrl Pts',(-21.8396080787796,20.8189771177922,-72.5150533772497));
#7473=CARTESIAN_POINT('Ctrl Pts',(-21.825914074999,20.8275967373245,-72.5140538436102));
#7474=CARTESIAN_POINT('Ctrl Pts',(-21.8183585410633,20.8323965953965,-72.513499732258));
#7475=CARTESIAN_POINT('Ctrl Pts',(-21.6645155785371,20.9310315127397,-72.5021629413938));
#7476=CARTESIAN_POINT('Ctrl Pts',(-21.5260610016184,21.0364997121222,-72.4909327575785));
#7477=CARTESIAN_POINT('Ctrl Pts',(-21.1598359467355,21.3654244957262,-72.4582007333772));
#7478=CARTESIAN_POINT('Ctrl Pts',(-20.9557444641652,21.612189705943,-72.4359696888479));
#7479=CARTESIAN_POINT('Ctrl Pts',(-20.7826992529491,21.8988790799341,-72.4147743795314));
#7480=CARTESIAN_POINT('Ctrl Pts',(-20.7743483134476,21.9129556050497,-72.4137447368886));
#7481=CARTESIAN_POINT('Ctrl Pts',(-20.7642922182614,21.9302044936042,-72.4124970517785));
#7482=CARTESIAN_POINT('Ctrl Pts',(-20.7624848677775,21.933316550873,-72.4122724960208));
#7483=CARTESIAN_POINT('Ctrl Pts',(-20.759516385288,21.9384477207615,-72.4119031654202));
#7484=CARTESIAN_POINT('Ctrl Pts',(-20.7583522291408,21.9404650649528,-72.411758194431));
#7485=CARTESIAN_POINT('Ctrl Pts',(-20.7562587112814,21.9441019843636,-72.4114972592962));
#7486=CARTESIAN_POINT('Ctrl Pts',(-20.7553285723107,21.9457211014882,-72.4113812444837));
#7487=CARTESIAN_POINT('Ctrl Pts',(-20.753333194273,21.9492015076725,-72.4111321864348));
#7488=CARTESIAN_POINT('Ctrl Pts',(-20.752268408661,21.9510630467112,-72.4109991730698));
#7489=CARTESIAN_POINT('Ctrl Pts',(-20.7493615998514,21.9561567408984,-72.4106357496681));
#7490=CARTESIAN_POINT('Ctrl Pts',(-20.74752330652,21.9593910377238,-72.410405582289));
#7491=CARTESIAN_POINT('Ctrl Pts',(-20.7380636555902,21.9761016548405,-72.4092193941321));
#7492=CARTESIAN_POINT('Ctrl Pts',(-20.7305337104048,21.989629883668,-72.4082692143598));
#7493=CARTESIAN_POINT('Ctrl Pts',(-20.6858243713992,22.0713343192976,-72.4025879111214));
#7494=CARTESIAN_POINT('Ctrl Pts',(-20.6510182979625,22.1407878131696,-72.3979972146846));
#7495=CARTESIAN_POINT('Ctrl Pts',(-20.5558119212181,22.3492537778529,-72.38471273206));
#7496=CARTESIAN_POINT('Ctrl Pts',(-20.5026636937856,22.491346944833,-72.3762784129801));
#7497=CARTESIAN_POINT('Ctrl Pts',(-20.4321144308882,22.7300044828328,-72.3623720505439));
#7498=CARTESIAN_POINT('Ctrl Pts',(-20.4087647976555,22.8245486955147,-72.3569283292848));
#7499=CARTESIAN_POINT('Ctrl Pts',(-20.3567085568718,23.0855956017489,-72.3418194569642));
#7500=CARTESIAN_POINT('Ctrl Pts',(-20.3367564655348,23.2535039972248,-72.3320017838661));
#7501=CARTESIAN_POINT('Ctrl Pts',(-20.3295937579461,23.4336106744,-72.3210400961515));
#7502=CARTESIAN_POINT('Ctrl Pts',(-20.3292002550901,23.4450361551618,-72.3203429676856));
#7503=CARTESIAN_POINT('Ctrl Pts',(-20.3287385702888,23.4608936861442,-72.3193729158071));
#7504=CARTESIAN_POINT('Ctrl Pts',(-20.3286187237968,23.4653242425301,-72.3191016148444));
#7505=CARTESIAN_POINT('Ctrl Pts',(-20.3284282492657,23.4729475866262,-72.3186343356407));
#7506=CARTESIAN_POINT('Ctrl Pts',(-20.3283532263996,23.4761402667875,-72.3184384955782));
#7507=CARTESIAN_POINT('Ctrl Pts',(-20.3282083454434,23.4827224073648,-72.3180344498135));
#7508=CARTESIAN_POINT('Ctrl Pts',(-20.3281390898806,23.4861118753894,-72.3178262254764));
#7509=CARTESIAN_POINT('Ctrl Pts',(-20.3279922754576,23.4938987655694,-72.3173474820785));
#7510=CARTESIAN_POINT('Ctrl Pts',(-20.3279183700067,23.4982962424339,-72.3170768486563));
#7511=CARTESIAN_POINT('Ctrl Pts',(-20.3277152302911,23.5120602295998,-72.3162289091511));
#7512=CARTESIAN_POINT('Ctrl Pts',(-20.3276178328424,23.5214270974915,-72.3156506046861));
#7513=CARTESIAN_POINT('Ctrl Pts',(-20.3274869753145,23.5430997129128,-72.3143096007185));
#7514=CARTESIAN_POINT('Ctrl Pts',(-20.3274831581506,23.5554054321558,-72.3135459771651));
#7515=CARTESIAN_POINT('Ctrl Pts',(-20.327706357012,23.5966068973697,-72.3109817248945));
#7516=CARTESIAN_POINT('Ctrl Pts',(-20.328251526394,23.6254988557357,-72.3091711751437));
#7517=CARTESIAN_POINT('Ctrl Pts',(-20.3313970666911,23.7228037324984,-72.3030302021037));
#7518=CARTESIAN_POINT('Ctrl Pts',(-20.3357886086877,23.7911362908748,-72.2986451292109));
#7519=CARTESIAN_POINT('Ctrl Pts',(-20.358224304757,24.0240380242361,-72.2834484585624));
#7520=CARTESIAN_POINT('Ctrl Pts',(-20.3867649108549,24.1873175893728,-72.2723483410731));
#7521=CARTESIAN_POINT('Ctrl Pts',(-20.4766193488191,24.5391728846557,-72.2477847368994));
#7522=CARTESIAN_POINT('Ctrl Pts',(-20.5430430290113,24.7257897630923,-72.2343271449293));
#7523=CARTESIAN_POINT('Ctrl Pts',(-20.6424340464649,24.9402916922294,-72.2191112340513));
#7524=CARTESIAN_POINT('Ctrl Pts',(-20.6593477803283,24.9751340227908,-72.2166491305541));
#7525=CARTESIAN_POINT('Ctrl Pts',(-20.6790383146339,25.0139017602392,-72.2139273461744));
#7526=CARTESIAN_POINT('Ctrl Pts',(-20.6811996501787,25.0181338989117,-72.2136304583473));
#7527=CARTESIAN_POINT('Ctrl Pts',(-20.6844690086226,25.0245008643299,-72.2131841901446));
#7528=CARTESIAN_POINT('Ctrl Pts',(-20.6855700614013,25.0266392330286,-72.2130343739313));
#7529=CARTESIAN_POINT('Ctrl Pts',(-20.6874813917749,25.0303410641366,-72.2127751346105));
#7530=CARTESIAN_POINT('Ctrl Pts',(-20.6882905567677,25.0319050947237,-72.2126656409976));
#7531=CARTESIAN_POINT('Ctrl Pts',(-20.6899794574327,25.0351630159769,-72.2124376378472));
#7532=CARTESIAN_POINT('Ctrl Pts',(-20.6908594151449,25.0368567866077,-72.2123191431937));
#7533=CARTESIAN_POINT('Ctrl Pts',(-20.6929544315746,25.0408805989838,-72.2120377400344));
#7534=CARTESIAN_POINT('Ctrl Pts',(-20.6941708399676,25.0432099450992,-72.2118749174835));
#7535=CARTESIAN_POINT('Ctrl Pts',(-20.69824274281,25.0509841956773,-72.211331748513));
#7536=CARTESIAN_POINT('Ctrl Pts',(-20.7011109919279,25.056422459367,-72.210952208355));
#7537=CARTESIAN_POINT('Ctrl Pts',(-20.7788648823567,25.2028286582762,-72.2007448251905));
#7538=CARTESIAN_POINT('Ctrl Pts',(-20.8641178122395,25.3380706058086,-72.19157214866));
#7539=CARTESIAN_POINT('Ctrl Pts',(-21.0969186923549,25.6528771362757,-72.1694878674436));
#7540=CARTESIAN_POINT('Ctrl Pts',(-21.2544891181059,25.8238722598998,-72.1567838214787));
#7541=CARTESIAN_POINT('Ctrl Pts',(-21.5169995937052,26.0533805382081,-72.1366356612996));
#7542=CARTESIAN_POINT('Ctrl Pts',(-21.6090632260881,26.1254314754588,-72.1297353287102));
#7543=CARTESIAN_POINT('Ctrl Pts',(-21.7135206279288,26.1983926178976,-72.1219822034176));
#7544=CARTESIAN_POINT('Ctrl Pts',(-21.7222436214134,26.2044215960496,-72.1213353499733));
#7545=CARTESIAN_POINT('Ctrl Pts',(-21.7345385552521,26.2128299927629,-72.1204243879174));
#7546=CARTESIAN_POINT('Ctrl Pts',(-21.7380858033918,26.2152455389987,-72.120161652897));
#7547=CARTESIAN_POINT('Ctrl Pts',(-21.7442508189623,26.2194256888055,-72.1197051772629));
#7548=CARTESIAN_POINT('Ctrl Pts',(-21.7468663804316,26.2211935490813,-72.1195115603052));
#7549=CARTESIAN_POINT('Ctrl Pts',(-21.7521346020615,26.2247430784347,-72.1191216721872));
#7550=CARTESIAN_POINT('Ctrl Pts',(-21.7547873223122,26.2265246507537,-72.118925397701));
#7551=CARTESIAN_POINT('Ctrl Pts',(-21.761100685248,26.2307511067096,-72.1184583814117));
#7552=CARTESIAN_POINT('Ctrl Pts',(-21.764763688993,26.2331924364598,-72.1181875059749));
#7553=CARTESIAN_POINT('Ctrl Pts',(-21.7762552512838,26.2408174107211,-72.1173379797739));
#7554=CARTESIAN_POINT('Ctrl Pts',(-21.7841014151399,26.2459743180915,-72.1167583252035));
#7555=CARTESIAN_POINT('Ctrl Pts',(-21.8023115259888,26.2578293225027,-72.1154138357312));
#7556=CARTESIAN_POINT('Ctrl Pts',(-21.8126915807703,26.2645022940685,-72.114648070505));
#7557=CARTESIAN_POINT('Ctrl Pts',(-21.8475969222775,26.2866594246915,-72.1120749071122));
#7558=CARTESIAN_POINT('Ctrl Pts',(-21.8722923072265,26.3018717285867,-72.1102575103772));
#7559=CARTESIAN_POINT('Ctrl Pts',(-21.9477822592086,26.3469792212305,-72.1047100262824));
#7560=CARTESIAN_POINT('Ctrl Pts',(-21.9991924265224,26.3758149498707,-72.1009426615874));
#7561=CARTESIAN_POINT('Ctrl Pts',(-22.0592366211213,26.4073609035813,-72.0965536886999));
#7562=CARTESIAN_POINT('Ctrl Pts',(-22.0671281311305,26.4114653315986,-72.095977076891));
#7563=CARTESIAN_POINT('Ctrl Pts',(-22.0750360205127,26.4155367772164,-72.0953994964366));
#7564=CARTESIAN_POINT('Origin',(-23.5502525316942,23.5502525316942,-77.3107734492734));
#7565=CARTESIAN_POINT('',(-22.0750359531635,26.415536742541,-70.5966750543042));
#7566=CARTESIAN_POINT('',(-22.0750360699906,26.4155368026905,-70.8406447795461));
#7567=CARTESIAN_POINT('',(-22.0750360153461,26.4155367745563,-77.3107734492734));
#7568=CARTESIAN_POINT('',(-26.7730024145035,23.5493834215643,-71.4421835438062));
#7569=CARTESIAN_POINT('Ctrl Pts',(-22.0750359531635,26.415536742541,-70.5966750543042));
#7570=CARTESIAN_POINT('Ctrl Pts',(-21.9892850292296,26.3713871310879,-70.6032038036302));
#7571=CARTESIAN_POINT('Ctrl Pts',(-21.9055397994592,26.3234003042188,-70.6097295152631));
#7572=CARTESIAN_POINT('Ctrl Pts',(-21.7599034326677,26.2310246085883,-70.6212244394833));
#7573=CARTESIAN_POINT('Ctrl Pts',(-21.6972050630861,26.1880746732894,-70.6262247757862));
#7574=CARTESIAN_POINT('Ctrl Pts',(-21.6063131854465,26.1209696179805,-70.633488007698));
#7575=CARTESIAN_POINT('Ctrl Pts',(-21.5769262927655,26.0984814004276,-70.6358385939486));
#7576=CARTESIAN_POINT('Ctrl Pts',(-21.5439017569547,26.0722954699336,-70.6384765743049));
#7577=CARTESIAN_POINT('Ctrl Pts',(-21.5398794458165,26.0690903728567,-70.6387978123834));
#7578=CARTESIAN_POINT('Ctrl Pts',(-21.5339503179122,26.0643426176988,-70.6392712232271));
#7579=CARTESIAN_POINT('Ctrl Pts',(-21.5320375873696,26.0628074099904,-70.6394239275884));
#7580=CARTESIAN_POINT('Ctrl Pts',(-21.528690250545,26.0601144610338,-70.6396911313837));
#7581=CARTESIAN_POINT('Ctrl Pts',(-21.5272548840587,26.058957671531,-70.6398056997738));
#7582=CARTESIAN_POINT('Ctrl Pts',(-21.5242671871098,26.0565455974481,-70.6400441486958));
#7583=CARTESIAN_POINT('Ctrl Pts',(-21.5227150332066,26.0552901043058,-70.6401680134129));
#7584=CARTESIAN_POINT('Ctrl Pts',(-21.5195499894223,26.0527251216449,-70.6404205652415));
#7585=CARTESIAN_POINT('Ctrl Pts',(-21.5179371967983,26.0514155128392,-70.6405492435975));
#7586=CARTESIAN_POINT('Ctrl Pts',(-21.5139912669188,26.048205029417,-70.6408640451094));
#7587=CARTESIAN_POINT('Ctrl Pts',(-21.5116595179733,26.0463024398264,-70.641050044644));
#7588=CARTESIAN_POINT('Ctrl Pts',(-21.5052616076968,26.0410671221099,-70.6415603379586));
#7589=CARTESIAN_POINT('Ctrl Pts',(-21.5012009089658,26.037727687623,-70.6418841535717));
#7590=CARTESIAN_POINT('Ctrl Pts',(-21.355169040619,25.9170338642853,-70.6535277656782));
#7591=CARTESIAN_POINT('Ctrl Pts',(-21.2234864664741,25.7877125674087,-70.6639839209856));
#7592=CARTESIAN_POINT('Ctrl Pts',(-20.9009941774329,25.4115451061679,-70.6917743222833));
#7593=CARTESIAN_POINT('Ctrl Pts',(-20.7337473722454,25.147205145449,-70.7089016170191));
#7594=CARTESIAN_POINT('Ctrl Pts',(-20.5993451455506,24.8458663179146,-70.7288746408929));
#7595=CARTESIAN_POINT('Ctrl Pts',(-20.5918535332808,24.8286674986169,-70.7300152341073));
#7596=CARTESIAN_POINT('Ctrl Pts',(-20.5821448560426,24.8058364587985,-70.7315305193548));
#7597=CARTESIAN_POINT('Ctrl Pts',(-20.5797927856637,24.8002617591353,-70.7319006012072));
#7598=CARTESIAN_POINT('Ctrl Pts',(-20.5761663714328,24.7915986702821,-70.7324758626447));
#7599=CARTESIAN_POINT('Ctrl Pts',(-20.5748810989189,24.7885148469309,-70.7326806702083));
#7600=CARTESIAN_POINT('Ctrl Pts',(-20.5723178842173,24.7823377557452,-70.7330909753885));
#7601=CARTESIAN_POINT('Ctrl Pts',(-20.5710399606582,24.7792444846443,-70.7332964733336));
#7602=CARTESIAN_POINT('Ctrl Pts',(-20.5681983627368,24.7723357933626,-70.7337555172112));
#7603=CARTESIAN_POINT('Ctrl Pts',(-20.5666371898208,24.768519356545,-70.7340091475854));
#7604=CARTESIAN_POINT('Ctrl Pts',(-20.5620949374191,24.7573542853407,-70.7347512997315));
#7605=CARTESIAN_POINT('Ctrl Pts',(-20.5591336687111,24.7499976702905,-70.7352404911954));
#7606=CARTESIAN_POINT('Ctrl Pts',(-20.537699307516,24.6961761246824,-70.7388209476672));
#7607=CARTESIAN_POINT('Ctrl Pts',(-20.5202835494736,24.6492999929661,-70.7419476507049));
#7608=CARTESIAN_POINT('Ctrl Pts',(-20.4671317143038,24.4953565749744,-70.7522504601279));
#7609=CARTESIAN_POINT('Ctrl Pts',(-20.4359308090597,24.3868235280148,-70.7595712548786));
#7610=CARTESIAN_POINT('Ctrl Pts',(-20.3340723534792,23.946696683913,-70.7894439984553));
#7611=CARTESIAN_POINT('Ctrl Pts',(-20.3102229057037,23.6065552108426,-70.8131971284455));
#7612=CARTESIAN_POINT('Ctrl Pts',(-20.3401054464487,23.2654976471702,-70.8348416262284));
#7613=CARTESIAN_POINT('Ctrl Pts',(-20.3404145506776,23.2620342306911,-70.8350611693359));
#7614=CARTESIAN_POINT('Ctrl Pts',(-20.3418240516454,23.2465247439172,-70.8360431389173));
#7615=CARTESIAN_POINT('Ctrl Pts',(-20.3429866771223,23.2344842150292,-70.8368023291684));
#7616=CARTESIAN_POINT('Ctrl Pts',(-20.3445800802736,23.2189001025309,-70.8377806275089));
#7617=CARTESIAN_POINT('Ctrl Pts',(-20.3449489694734,23.2153504976337,-70.8380031643972));
#7618=CARTESIAN_POINT('Ctrl Pts',(-20.3455232900249,23.2099120257479,-70.8383436674066));
#7619=CARTESIAN_POINT('Ctrl Pts',(-20.3457244953918,23.2080227302547,-70.8384618724142));
#7620=CARTESIAN_POINT('Ctrl Pts',(-20.3461224479411,23.2043171236231,-70.8386935500811));
#7621=CARTESIAN_POINT('Ctrl Pts',(-20.346319067803,23.2025008111201,-70.8388070290018));
#7622=CARTESIAN_POINT('Ctrl Pts',(-20.346756910027,23.1984880551759,-70.8390575635751));
#7623=CARTESIAN_POINT('Ctrl Pts',(-20.3469988462892,23.1962916977149,-70.8391945778825));
#7624=CARTESIAN_POINT('Ctrl Pts',(-20.3475060538636,23.1917302517588,-70.8394788982338));
#7625=CARTESIAN_POINT('Ctrl Pts',(-20.3477716866329,23.1893652036136,-70.8396261837204));
#7626=CARTESIAN_POINT('Ctrl Pts',(-20.3484606741315,23.1832915029774,-70.8400040979049));
#7627=CARTESIAN_POINT('Ctrl Pts',(-20.3488878542187,23.179583274952,-70.8402345120502));
#7628=CARTESIAN_POINT('Ctrl Pts',(-20.3501464650398,23.1688221195246,-70.8409022677099));
#7629=CARTESIAN_POINT('Ctrl Pts',(-20.3509947737307,23.161771132547,-70.8413386776453));
#7630=CARTESIAN_POINT('Ctrl Pts',(-20.3539574440431,23.1378139783144,-70.8428178327285));
#7631=CARTESIAN_POINT('Ctrl Pts',(-20.3561826035084,23.1209214589807,-70.8438546464765));
#7632=CARTESIAN_POINT('Ctrl Pts',(-20.3657315971399,23.0526174547791,-70.8480248737247));
#7633=CARTESIAN_POINT('Ctrl Pts',(-20.3741639689777,23.0013660699005,-70.8511032926738));
#7634=CARTESIAN_POINT('Ctrl Pts',(-20.3967037709155,22.8823983212118,-70.8581770549293));
#7635=CARTESIAN_POINT('Ctrl Pts',(-20.4117596443322,22.8148870398657,-70.8621363831965));
#7636=CARTESIAN_POINT('Ctrl Pts',(-20.4968242824211,22.4839685750669,-70.8814943166409));
#7637=CARTESIAN_POINT('Ctrl Pts',(-20.5978707671488,22.229711104634,-70.8963157456147));
#7638=CARTESIAN_POINT('Ctrl Pts',(-20.7745337107521,21.9101037587168,-70.9176288425984));
#7639=CARTESIAN_POINT('Ctrl Pts',(-20.8228307861055,21.8309878436158,-70.9231396822197));
#7640=CARTESIAN_POINT('Ctrl Pts',(-20.880161711729,21.7455816386368,-70.9294015139037));
#7641=CARTESIAN_POINT('Ctrl Pts',(-20.8858982885614,21.737123059641,-70.9300251861296));
#7642=CARTESIAN_POINT('Ctrl Pts',(-20.8940014723468,21.7252964185789,-70.9309021784169));
#7643=CARTESIAN_POINT('Ctrl Pts',(-20.8963344868586,21.7219053228409,-70.9311542198023));
#7644=CARTESIAN_POINT('Ctrl Pts',(-20.9006205713289,21.715700878964,-70.9316164267244));
#7645=CARTESIAN_POINT('Ctrl Pts',(-20.9025716443979,21.7128861526524,-70.9318265158399));
#7646=CARTESIAN_POINT('Ctrl Pts',(-20.9065286760029,21.7071969101552,-70.9322519756317));
#7647=CARTESIAN_POINT('Ctrl Pts',(-20.9085348443187,21.704322546757,-70.9324673541369));
#7648=CARTESIAN_POINT('Ctrl Pts',(-20.9134743060289,21.6972700135559,-70.9329968534213));
#7649=CARTESIAN_POINT('Ctrl Pts',(-20.9164128381189,21.6930955399629,-70.933311175083));
#7650=CARTESIAN_POINT('Ctrl Pts',(-20.9271028272931,21.677985761959,-70.9344521840119));
#7651=CARTESIAN_POINT('Ctrl Pts',(-20.9349124867696,21.6670919784106,-70.9352811123814));
#7652=CARTESIAN_POINT('Ctrl Pts',(-21.0489977158415,21.5100316970904,-70.9473245323954));
#7653=CARTESIAN_POINT('Ctrl Pts',(-21.1672965071065,21.3730347818828,-70.9590228718309));
#7654=CARTESIAN_POINT('Ctrl Pts',(-21.3227766837434,21.220911968814,-70.9735148075534));
#7655=CARTESIAN_POINT('Ctrl Pts',(-21.3495622263754,21.1955894585539,-70.9759823219047));
#7656=CARTESIAN_POINT('Ctrl Pts',(-21.579982798918,20.9851210645971,-70.9969502185605));
#7657=CARTESIAN_POINT('Ctrl Pts',(-21.8061342493775,20.8262977913076,-71.0159702208884));
#7658=CARTESIAN_POINT('Ctrl Pts',(-22.0635271434046,20.6908805017038,-71.034366750045));
#7659=CARTESIAN_POINT('Ctrl Pts',(-22.0773820235936,20.683719211485,-71.0353474863602));
#7660=CARTESIAN_POINT('Ctrl Pts',(-22.0944417081503,20.675057770836,-71.0365429535999));
#7661=CARTESIAN_POINT('Ctrl Pts',(-22.0975973939008,20.6734621121898,-71.0367635838509));
#7662=CARTESIAN_POINT('Ctrl Pts',(-22.1028185133072,20.6708328576766,-71.0371277749874));
#7663=CARTESIAN_POINT('Ctrl Pts',(-22.1048824319863,20.6697962880334,-71.0372715227895));
#7664=CARTESIAN_POINT('Ctrl Pts',(-22.108578404195,20.6679450186253,-71.0375285480613));
#7665=CARTESIAN_POINT('Ctrl Pts',(-22.1102100309623,20.6671294878519,-71.0376418780262));
#7666=CARTESIAN_POINT('Ctrl Pts',(-22.1137209660678,20.6653783523669,-71.0378854474643));
#7667=CARTESIAN_POINT('Ctrl Pts',(-22.1156004912948,20.6644432010854,-71.0380156579382));
#7668=CARTESIAN_POINT('Ctrl Pts',(-22.1194738573454,20.6625207405351,-71.0382836292246));
#7669=CARTESIAN_POINT('Ctrl Pts',(-22.1214678102611,20.661533657779,-71.0384213757156));
#7670=CARTESIAN_POINT('Ctrl Pts',(-22.1264786917714,20.6590595377337,-71.0387670367515));
#7671=CARTESIAN_POINT('Ctrl Pts',(-22.1294969379766,20.6575751527361,-71.0389747857966));
#7672=CARTESIAN_POINT('Ctrl Pts',(-22.1380375392721,20.6533914442138,-71.0395613718558));
#7673=CARTESIAN_POINT('Ctrl Pts',(-22.1435653374531,20.6507031729179,-71.0399395305982));
#7674=CARTESIAN_POINT('Ctrl Pts',(-22.1617184304461,20.641939116138,-71.0411765819042));
#7675=CARTESIAN_POINT('Ctrl Pts',(-22.174375866046,20.6359297474945,-71.0420315212618));
#7676=CARTESIAN_POINT('Ctrl Pts',(-22.2259836667265,20.6118390900819,-71.0454881222256));
#7677=CARTESIAN_POINT('Ctrl Pts',(-22.2652562310139,20.5944537428358,-71.0480512321415));
#7678=CARTESIAN_POINT('Ctrl Pts',(-22.3780010824317,20.5472154521471,-71.0552518989229));
#7679=CARTESIAN_POINT('Ctrl Pts',(-22.4522464012086,20.5192808563478,-71.0598069040343));
#7680=CARTESIAN_POINT('Ctrl Pts',(-22.863831542639,20.3815352502135,-71.0844264581023));
#7681=CARTESIAN_POINT('Ctrl Pts',(-23.2164546255123,20.3252680465064,-71.1035609964176));
#7682=CARTESIAN_POINT('Ctrl Pts',(-23.5921915047673,20.3277068608455,-71.1262757346744));
#7683=CARTESIAN_POINT('Ctrl Pts',(-23.6132106148638,20.3280489804896,-71.1275528394202));
#7684=CARTESIAN_POINT('Ctrl Pts',(-23.6405512317939,20.3287616094564,-71.1292228509764));
#7685=CARTESIAN_POINT('Ctrl Pts',(-23.6468774337668,20.3289451504129,-71.129609880202));
#7686=CARTESIAN_POINT('Ctrl Pts',(-23.6569755599138,20.3292678989532,-71.1302286651942));
#7687=CARTESIAN_POINT('Ctrl Pts',(-23.6607478736644,20.329395101084,-71.1304600435583));
#7688=CARTESIAN_POINT('Ctrl Pts',(-23.6675368968589,20.3296359674851,-71.1308768564353));
#7689=CARTESIAN_POINT('Ctrl Pts',(-23.670553691065,20.3297472441774,-71.1310622157031));
#7690=CARTESIAN_POINT('Ctrl Pts',(-23.6776209163499,20.3300178681161,-71.1314967801037));
#7691=CARTESIAN_POINT('Ctrl Pts',(-23.6816712054322,20.3301806185415,-71.1317460919112));
#7692=CARTESIAN_POINT('Ctrl Pts',(-23.693314937081,20.3306704969953,-71.1324635619173));
#7693=CARTESIAN_POINT('Ctrl Pts',(-23.7009075053963,20.3310168448729,-71.1329323233742));
#7694=CARTESIAN_POINT('Ctrl Pts',(-23.7510490196824,20.3334819094208,-71.1360341852083));
#7695=CARTESIAN_POINT('Ctrl Pts',(-23.7935519016257,20.3364171903181,-71.1386928443388));
#7696=CARTESIAN_POINT('Ctrl Pts',(-23.9181342268814,20.347506367367,-71.1465766656584));
#7697=CARTESIAN_POINT('Ctrl Pts',(-23.9999684168833,20.3579690844458,-71.1518724480335));
#7698=CARTESIAN_POINT('Ctrl Pts',(-24.1751966935086,20.3872438516674,-71.1634659980193));
#7699=CARTESIAN_POINT('Ctrl Pts',(-24.2683400513007,20.407081021823,-71.1697871080189));
#7700=CARTESIAN_POINT('Ctrl Pts',(-24.3886318233353,20.4383263230843,-71.1781280163419));
#7701=CARTESIAN_POINT('Ctrl Pts',(-24.4166996635281,20.4460241422021,-71.1800868722044));
#7702=CARTESIAN_POINT('Ctrl Pts',(-24.468334272944,20.4609401860885,-71.1837117834367));
#7703=CARTESIAN_POINT('Ctrl Pts',(-24.4919301007552,20.4680506898726,-71.1853765939769));
#7704=CARTESIAN_POINT('Ctrl Pts',(-24.5358229932785,20.4818287105749,-71.1884875015241));
#7705=CARTESIAN_POINT('Ctrl Pts',(-24.5561399142455,20.4884288185778,-71.1899331289735));
#7706=CARTESIAN_POINT('Ctrl Pts',(-24.6434728607559,20.5177626747209,-71.196169134661));
#7707=CARTESIAN_POINT('Ctrl Pts',(-24.7097965410869,20.542498657975,-71.2009614615115));
#7708=CARTESIAN_POINT('Ctrl Pts',(-24.8742539360703,20.6100834295595,-71.2129222777329));
#7709=CARTESIAN_POINT('Ctrl Pts',(-24.9711759180797,20.6556791904232,-71.2200440030226));
#7710=CARTESIAN_POINT('Ctrl Pts',(-25.1018714970696,20.7253135924841,-71.2295898559903));
#7711=CARTESIAN_POINT('Ctrl Pts',(-25.1377171200278,20.7453001257383,-71.2322014345765));
#7712=CARTESIAN_POINT('Ctrl Pts',(-25.1773470867849,20.7683998736378,-71.2350730827209));
#7713=CARTESIAN_POINT('Ctrl Pts',(-25.1815154862095,20.7708421488451,-71.235374934865));
#7714=CARTESIAN_POINT('Ctrl Pts',(-25.1877681537444,20.7745245133703,-71.2358274040225));
#7715=CARTESIAN_POINT('Ctrl Pts',(-25.1898565159266,20.7757575832124,-71.235978473886));
#7716=CARTESIAN_POINT('Ctrl Pts',(-25.1934632645777,20.7778926760953,-71.2362392882517));
#7717=CARTESIAN_POINT('Ctrl Pts',(-25.1949823011349,20.7787935897017,-71.2363491053102));
#7718=CARTESIAN_POINT('Ctrl Pts',(-25.1981051678671,20.7806491782135,-71.2365748088885));
#7719=CARTESIAN_POINT('Ctrl Pts',(-25.1997089070507,20.7816039964039,-71.236690685213));
#7720=CARTESIAN_POINT('Ctrl Pts',(-25.203482301078,20.7838550042931,-71.2369632514795));
#7721=CARTESIAN_POINT('Ctrl Pts',(-25.2056512683338,20.7851523575912,-71.237119864896));
#7722=CARTESIAN_POINT('Ctrl Pts',(-25.210239193625,20.7879039275634,-71.2374510223126));
#7723=CARTESIAN_POINT('Ctrl Pts',(-25.212657774047,20.7893587744348,-71.2376255249954));
#7724=CARTESIAN_POINT('Ctrl Pts',(-25.2191823694586,20.7932951913422,-71.238096097238));
#7725=CARTESIAN_POINT('Ctrl Pts',(-25.2232847793813,20.7957827680566,-71.2383917786249));
#7726=CARTESIAN_POINT('Ctrl Pts',(-25.2359309008559,20.803489667227,-71.2393026917029));
#7727=CARTESIAN_POINT('Ctrl Pts',(-25.2444559557694,20.8087397081276,-71.2399159736936));
#7728=CARTESIAN_POINT('Ctrl Pts',(-25.2760210822053,20.828382137102,-71.2421843383901));
#7729=CARTESIAN_POINT('Ctrl Pts',(-25.2989040850165,20.8430263888306,-71.2438240251639));
#7730=CARTESIAN_POINT('Ctrl Pts',(-25.3934156206076,20.9052085966818,-71.2505883138839));
#7731=CARTESIAN_POINT('Ctrl Pts',(-25.4633179034705,20.9553169157508,-71.2555723900795));
#7732=CARTESIAN_POINT('Ctrl Pts',(-25.7679162563114,21.1926707687169,-71.2776021714226));
#7733=CARTESIAN_POINT('Ctrl Pts',(-25.977750902946,21.4093445452344,-71.2938002440374));
#7734=CARTESIAN_POINT('Ctrl Pts',(-26.166841485475,21.668760224476,-71.312597940705));
#7735=CARTESIAN_POINT('Ctrl Pts',(-26.1789419793269,21.6857035739098,-71.313822471663));
#7736=CARTESIAN_POINT('Ctrl Pts',(-26.1938703911685,21.7070408139461,-71.3153612480714));
#7737=CARTESIAN_POINT('Ctrl Pts',(-26.196853106376,21.7113261544222,-71.3156701281165));
#7738=CARTESIAN_POINT('Ctrl Pts',(-26.2021170900613,21.7189283843995,-71.3162178053392));
#7739=CARTESIAN_POINT('Ctrl Pts',(-26.2044025869117,21.7222423422886,-71.3164564549917));
#7740=CARTESIAN_POINT('Ctrl Pts',(-26.2090961134865,21.7290752882695,-71.3169483346181));
#7741=CARTESIAN_POINT('Ctrl Pts',(-26.2115033795865,21.7325947892271,-71.3172015905934));
#7742=CARTESIAN_POINT('Ctrl Pts',(-26.2435751425151,21.7796850324163,-71.3205888217182));
#7743=CARTESIAN_POINT('Ctrl Pts',(-26.2721719186701,21.8239703092295,-71.3237598136174));
#7744=CARTESIAN_POINT('Ctrl Pts',(-26.3042183443168,21.8763750217552,-71.3275032315013));
#7745=CARTESIAN_POINT('Ctrl Pts',(-26.3087377715978,21.8838333784637,-71.328035790609));
#7746=CARTESIAN_POINT('Ctrl Pts',(-26.3154329563237,21.8949842304217,-71.3288317284853));
#7747=CARTESIAN_POINT('Ctrl Pts',(-26.3176317366415,21.8986629138726,-71.3290942641381));
#7748=CARTESIAN_POINT('Ctrl Pts',(-26.3215424129114,21.9052354309832,-71.3295632468334));
#7749=CARTESIAN_POINT('Ctrl Pts',(-26.3232571336195,21.9081275836668,-71.3297695903778));
#7750=CARTESIAN_POINT('Ctrl Pts',(-26.3268648073566,21.9142342708926,-71.3302052251803));
#7751=CARTESIAN_POINT('Ctrl Pts',(-26.3287567099964,21.9174494174132,-71.3304345543032));
#7752=CARTESIAN_POINT('Ctrl Pts',(-26.3337439007024,21.925958540991,-71.3310414135238));
#7753=CARTESIAN_POINT('Ctrl Pts',(-26.3368296569134,21.9312580616756,-71.3314192892863));
#7754=CARTESIAN_POINT('Ctrl Pts',(-26.3507682883173,21.9553543644333,-71.3331371193073));
#7755=CARTESIAN_POINT('Ctrl Pts',(-26.3614460234371,21.974251331858,-71.3344833921636));
#7756=CARTESIAN_POINT('Ctrl Pts',(-26.4386132310049,22.1140980681876,-71.3444417768299));
#7757=CARTESIAN_POINT('Ctrl Pts',(-26.4974536756728,22.2390837798798,-71.3533257501392));
#7758=CARTESIAN_POINT('Ctrl Pts',(-26.6675128583361,22.6701002962163,-71.3839028677412));
#7759=CARTESIAN_POINT('Ctrl Pts',(-26.7403957530622,22.989057686152,-71.406635760132));
#7760=CARTESIAN_POINT('Ctrl Pts',(-26.7651345498603,23.3249042087348,-71.4282245839749));
#7761=CARTESIAN_POINT('Ctrl Pts',(-26.7659137220449,23.3363100755452,-71.4289547380944));
#7762=CARTESIAN_POINT('Ctrl Pts',(-26.7670031026628,23.3536103190369,-71.4300573828326));
#7763=CARTESIAN_POINT('Ctrl Pts',(-26.7673578308445,23.3595016706257,-71.4304320220343));
#7764=CARTESIAN_POINT('Ctrl Pts',(-26.7686820702394,23.3825499236053,-71.4318942787692));
#7765=CARTESIAN_POINT('Ctrl Pts',(-26.7695305580163,23.3997138995711,-71.4329758216672));
#7766=CARTESIAN_POINT('Ctrl Pts',(-26.7703932948379,23.4205434702407,-71.4342787053149));
#7767=CARTESIAN_POINT('Ctrl Pts',(-26.7705386173413,23.4242029303488,-71.4345072428034));
#7768=CARTESIAN_POINT('Ctrl Pts',(-26.770766902714,23.4302097665429,-71.434881775814));
#7769=CARTESIAN_POINT('Ctrl Pts',(-26.7708535374045,23.4325569858945,-71.4350279770372));
#7770=CARTESIAN_POINT('Ctrl Pts',(-26.7710010603859,23.4366760355387,-71.4352842735568));
#7771=CARTESIAN_POINT('Ctrl Pts',(-26.7710630526366,23.4384478189484,-71.4353944312232));
#7772=CARTESIAN_POINT('Ctrl Pts',(-26.7711833829345,23.4419701154023,-71.4356132512964));
#7773=CARTESIAN_POINT('Ctrl Pts',(-26.7712417557756,23.4437206184636,-71.435721915374));
#7774=CARTESIAN_POINT('Ctrl Pts',(-26.7713657670809,23.4475328055368,-71.4359583777471));
#7775=CARTESIAN_POINT('Ctrl Pts',(-26.7714308533296,23.44959450862,-71.4360861447737));
#7776=CARTESIAN_POINT('Ctrl Pts',(-26.7715849287522,23.4546283118795,-71.4363978167068));
#7777=CARTESIAN_POINT('Ctrl Pts',(-26.7716717844036,23.4576004826506,-71.4365816019813));
#7778=CARTESIAN_POINT('Ctrl Pts',(-26.772036872106,23.4707152692677,-71.4373915216383));
#7779=CARTESIAN_POINT('Ctrl Pts',(-26.7722713216653,23.4808591907938,-71.4380152327469));
#7780=CARTESIAN_POINT('Ctrl Pts',(-26.7728156331387,23.5104614351481,-71.4398278091507));
#7781=CARTESIAN_POINT('Ctrl Pts',(-26.7729971661461,23.5299219717071,-71.4410098780681));
#7782=CARTESIAN_POINT('Ctrl Pts',(-26.7730024145035,23.5493834215643,-71.4421835438062));
#7783=CARTESIAN_POINT('Ctrl Pts',(-26.7730024138161,23.5493808760687,-71.4421833902944));
#7784=CARTESIAN_POINT('Ctrl Pts',(-26.7730886644055,23.8682729577653,-71.4614148940303));
#7785=CARTESIAN_POINT('Ctrl Pts',(-26.7258452154471,24.1854881446483,-71.4784165817878));
#7786=CARTESIAN_POINT('Ctrl Pts',(-26.5851120910655,24.6467884258757,-71.5058464668276));
#7787=CARTESIAN_POINT('Ctrl Pts',(-26.5256933700641,24.7990534522733,-71.5153592880398));
#7788=CARTESIAN_POINT('Ctrl Pts',(-26.4503352561812,24.9558676944753,-71.5259462116029));
#7789=CARTESIAN_POINT('Ctrl Pts',(-26.4456168559279,24.9655614097221,-71.5266039281923));
#7790=CARTESIAN_POINT('Ctrl Pts',(-26.4387830660695,24.979423887874,-71.5275492570845));
#7791=CARTESIAN_POINT('Ctrl Pts',(-26.4367070723881,24.9836120809651,-71.5278354900792));
#7792=CARTESIAN_POINT('Ctrl Pts',(-26.4330958662347,24.9908578129591,-71.5283317752795));
#7793=CARTESIAN_POINT('Ctrl Pts',(-26.4315648793972,24.9939174591413,-71.5285416789351));
#7794=CARTESIAN_POINT('Ctrl Pts',(-26.4286170420225,24.999785284529,-71.5289448861996));
#7795=CARTESIAN_POINT('Ctrl Pts',(-26.4272009460425,25.0025938403817,-71.5291381630989));
#7796=CARTESIAN_POINT('Ctrl Pts',(-26.42386338162,25.0091892259508,-71.5295927165369));
#7797=CARTESIAN_POINT('Ctrl Pts',(-26.4219385389692,25.0129743336827,-71.5298541117765));
#7798=CARTESIAN_POINT('Ctrl Pts',(-26.4152980251481,25.0259689460633,-71.5307533219502));
#7799=CARTESIAN_POINT('Ctrl Pts',(-26.4105455252151,25.0351594656148,-71.5313924362837));
#7800=CARTESIAN_POINT('Ctrl Pts',(-26.3568149188174,25.1378501743489,-71.5385692384689));
#7801=CARTESIAN_POINT('Ctrl Pts',(-26.3033212168519,25.228902978184,-71.5452678261338));
#7802=CARTESIAN_POINT('Ctrl Pts',(-26.0888247736793,25.5560921159573,-71.5706531916715));
#7803=CARTESIAN_POINT('Ctrl Pts',(-25.9011177900716,25.7731175462074,-71.5903136845913));
#7804=CARTESIAN_POINT('Ctrl Pts',(-25.6544581696233,25.9916383244703,-71.612319335704));
#7805=CARTESIAN_POINT('Ctrl Pts',(-25.6209954240948,26.0200845325445,-71.6152321848534));
#7806=CARTESIAN_POINT('Ctrl Pts',(-25.5468077257184,26.0805824129723,-71.6215173224361));
#7807=CARTESIAN_POINT('Ctrl Pts',(-25.5058684935094,26.1123549560295,-71.6248772495191));
#7808=CARTESIAN_POINT('Ctrl Pts',(-25.4510367144948,26.1528289204955,-71.629218625523));
#7809=CARTESIAN_POINT('Ctrl Pts',(-25.437821079231,26.1624296645058,-71.6302532059088));
#7810=CARTESIAN_POINT('Ctrl Pts',(-25.4189325863508,26.1759333588546,-71.6317145578727));
#7811=CARTESIAN_POINT('Ctrl Pts',(-25.4133195929927,26.1799190656732,-71.6321466670537));
#7812=CARTESIAN_POINT('Ctrl Pts',(-25.4047114217467,26.185990209573,-71.6328060148139));
#7813=CARTESIAN_POINT('Ctrl Pts',(-25.4017254437196,26.1880885648532,-71.6330341151765));
#7814=CARTESIAN_POINT('Ctrl Pts',(-25.3961867181843,26.1919667906402,-71.6334560782462));
#7815=CARTESIAN_POINT('Ctrl Pts',(-25.3936349491107,26.1937480414553,-71.6336500345758));
#7816=CARTESIAN_POINT('Ctrl Pts',(-25.3894465629054,26.1966627117538,-71.6339676485371));
#7817=CARTESIAN_POINT('Ctrl Pts',(-25.3878114760881,26.1977983106177,-71.6340914562212));
#7818=CARTESIAN_POINT('Ctrl Pts',(-25.3846531207463,26.1999875131186,-71.6343302475276));
#7819=CARTESIAN_POINT('Ctrl Pts',(-25.3831299999663,26.2010413160398,-71.6344452446364));
#7820=CARTESIAN_POINT('Ctrl Pts',(-25.3795726712496,26.2034979963202,-71.6347134542611));
#7821=CARTESIAN_POINT('Ctrl Pts',(-25.3775377519226,26.2048998515042,-71.6348665962116));
#7822=CARTESIAN_POINT('Ctrl Pts',(-25.37102332315,26.2093765995646,-71.6353559532954));
#7823=CARTESIAN_POINT('Ctrl Pts',(-25.3665376186558,26.2124425262755,-71.6356915565095));
#7824=CARTESIAN_POINT('Ctrl Pts',(-25.3265419136952,26.239630981341,-71.6386720186872));
#7825=CARTESIAN_POINT('Ctrl Pts',(-25.2905588844853,26.2630545245981,-71.6412704082359));
#7826=CARTESIAN_POINT('Ctrl Pts',(-25.1766337532785,26.3340151738519,-71.6492764461011));
#7827=CARTESIAN_POINT('Ctrl Pts',(-25.0971289375772,26.3789671573703,-71.6545490450781));
#7828=CARTESIAN_POINT('Ctrl Pts',(-24.9439828394529,26.4571647827935,-71.6643271098377));
#7829=CARTESIAN_POINT('Ctrl Pts',(-24.8707952899996,26.4911351475046,-71.6688468490953));
#7830=CARTESIAN_POINT('Ctrl Pts',(-24.6405984485013,26.5876540626487,-71.6828032991666));
#7831=CARTESIAN_POINT('Ctrl Pts',(-24.4798966767702,26.6406279397683,-71.6921986279449));
#7832=CARTESIAN_POINT('Ctrl Pts',(-24.2048693763618,26.7078835943865,-71.7085062335232));
#7833=CARTESIAN_POINT('Ctrl Pts',(-24.0925947299074,26.7290915832619,-71.7152205745176));
#7834=CARTESIAN_POINT('Ctrl Pts',(-23.9602779342084,26.7468711420569,-71.7233011779076));
#7835=CARTESIAN_POINT('Ctrl Pts',(-23.9410935791098,26.7492734164506,-71.7244767290504));
#7836=CARTESIAN_POINT('Ctrl Pts',(-23.9160486237774,26.7521809119483,-71.7260169136057));
#7837=CARTESIAN_POINT('Ctrl Pts',(-23.9102063442367,26.7528429496796,-71.7263765855721));
#7838=CARTESIAN_POINT('Ctrl Pts',(-23.900710636706,26.7538926764132,-71.7269618213445));
#7839=CARTESIAN_POINT('Ctrl Pts',(-23.8970582817307,26.7542901144618,-71.7271870769296));
#7840=CARTESIAN_POINT('Ctrl Pts',(-23.8900478977173,26.7550408356108,-71.7276197364193));
#7841=CARTESIAN_POINT('Ctrl Pts',(-23.8866899755974,26.7553950885695,-71.7278271094012));
#7842=CARTESIAN_POINT('Ctrl Pts',(-23.8790312450713,26.756190898553,-71.7283003889381));
#7843=CARTESIAN_POINT('Ctrl Pts',(-23.8747300990827,26.7566290788948,-71.7285664016972));
#7844=CARTESIAN_POINT('Ctrl Pts',(-23.8613253039041,26.7579674473011,-71.7293961365713));
#7845=CARTESIAN_POINT('Ctrl Pts',(-23.8522187545565,26.7588375230727,-71.729960807284));
#7846=CARTESIAN_POINT('Ctrl Pts',(-23.7814691751168,26.7652933545638,-71.7343556367807));
#7847=CARTESIAN_POINT('Ctrl Pts',(-23.719684175881,26.7691406451981,-71.7382402623672));
#7848=CARTESIAN_POINT('Ctrl Pts',(-23.6528221305453,26.7713737878153,-71.7424986762539));
#7849=CARTESIAN_POINT('Ctrl Pts',(-23.6478138991513,26.7715293667975,-71.7428179763202));
#7850=CARTESIAN_POINT('Ctrl Pts',(-23.6210474195426,26.772298379375,-71.7445262316271));
#7851=CARTESIAN_POINT('Ctrl Pts',(-23.5992841430064,26.7727030318216,-71.7459213885585));
#7852=CARTESIAN_POINT('Ctrl Pts',(-23.2802578205115,26.775402273929,-71.7664641318538));
#7853=CARTESIAN_POINT('Ctrl Pts',(-22.984104753239,26.7367720038835,-71.7868894697297));
#7854=CARTESIAN_POINT('Ctrl Pts',(-22.6162448270906,26.6358400929353,-71.8124173807241));
#7855=CARTESIAN_POINT('Ctrl Pts',(-22.5358663739045,26.610357744276,-71.8179913257021));
#7856=CARTESIAN_POINT('Ctrl Pts',(-22.4295361182046,26.5719968084711,-71.8252819327593));
#7857=CARTESIAN_POINT('Ctrl Pts',(-22.4026289581061,26.5618806657602,-71.8271194636155));
#7858=CARTESIAN_POINT('Ctrl Pts',(-22.3661423006381,26.5476029300757,-71.8295976565094));
#7859=CARTESIAN_POINT('Ctrl Pts',(-22.356443262228,26.5437531388497,-71.8302551039994));
#7860=CARTESIAN_POINT('Ctrl Pts',(-22.3421747597746,26.5380092357018,-71.8312201663332));
#7861=CARTESIAN_POINT('Ctrl Pts',(-22.3375908010134,26.5361516513995,-71.8315298817148));
#7862=CARTESIAN_POINT('Ctrl Pts',(-22.3303416000514,26.5331945682383,-71.8320191391405));
#7863=CARTESIAN_POINT('Ctrl Pts',(-22.3276735490418,26.5321020426277,-71.8321990941795));
#7864=CARTESIAN_POINT('Ctrl Pts',(-22.3226280956955,26.530028097366,-71.8325391779053));
#7865=CARTESIAN_POINT('Ctrl Pts',(-22.3202503974894,26.529047410097,-71.832699350572));
#7866=CARTESIAN_POINT('Ctrl Pts',(-22.3161419542084,26.5273471150587,-71.8329759488819));
#7867=CARTESIAN_POINT('Ctrl Pts',(-22.3144106606635,26.5266288428544,-71.8330924562878));
#7868=CARTESIAN_POINT('Ctrl Pts',(-22.3110588589118,26.5252348318882,-71.8333179160466));
#7869=CARTESIAN_POINT('Ctrl Pts',(-22.3094382787435,26.5245592803069,-71.8334268796861));
#7870=CARTESIAN_POINT('Ctrl Pts',(-22.3056175452596,26.5229629113973,-71.8336836714568));
#7871=CARTESIAN_POINT('Ctrl Pts',(-22.3034178568115,26.5220409738024,-71.8338314308702));
#7872=CARTESIAN_POINT('Ctrl Pts',(-22.2969109272122,26.5193052807897,-71.8342682836547));
#7873=CARTESIAN_POINT('Ctrl Pts',(-22.292606581973,26.5174845870342,-71.8345569556469));
#7874=CARTESIAN_POINT('Ctrl Pts',(-22.2546895845058,26.5013487589937,-71.8370972898839));
#7875=CARTESIAN_POINT('Ctrl Pts',(-22.2213169284143,26.4864716536712,-71.8393152796189));
#7876=CARTESIAN_POINT('Ctrl Pts',(-22.1501141730033,26.4532675792383,-71.8440238489258));
#7877=CARTESIAN_POINT('Ctrl Pts',(-22.1123848385938,26.4347661416304,-71.8465041983327));
#7878=CARTESIAN_POINT('Ctrl Pts',(-22.0750359824043,26.4155367575959,-71.8489552970435));
#7879=CARTESIAN_POINT('',(-26.7730014767856,23.5476449634564,-71.6875616724776));
#7880=CARTESIAN_POINT('Ctrl Pts',(-22.0750360205127,26.4155367772164,-72.0953994964366));
#7881=CARTESIAN_POINT('Ctrl Pts',(-22.1819509304425,26.470582848358,-72.0875905907636));
#7882=CARTESIAN_POINT('Ctrl Pts',(-22.2918594983669,26.519599931717,-72.0795991983618));
#7883=CARTESIAN_POINT('Ctrl Pts',(-22.6337869481824,26.6496917839157,-72.0549904497339));
#7884=CARTESIAN_POINT('Ctrl Pts',(-22.8725623929651,26.710502408185,-72.0380895041274));
#7885=CARTESIAN_POINT('Ctrl Pts',(-23.1522977768553,26.7485483776874,-72.0199440442071));
#7886=CARTESIAN_POINT('Ctrl Pts',(-23.1887447833961,26.7528728244459,-72.0176129189538));
#7887=CARTESIAN_POINT('Ctrl Pts',(-23.2299151189397,26.7570458523138,-72.015022870123));
#7888=CARTESIAN_POINT('Ctrl Pts',(-23.2345717110298,26.7575076009555,-72.0147305429394));
#7889=CARTESIAN_POINT('Ctrl Pts',(-23.2416048413163,26.7581895419619,-72.0142899790898));
#7890=CARTESIAN_POINT('Ctrl Pts',(-23.2439806201013,26.7584172367679,-72.0141413219657));
#7891=CARTESIAN_POINT('Ctrl Pts',(-23.2481050639217,26.7588079004803,-72.0138835356537));
#7892=CARTESIAN_POINT('Ctrl Pts',(-23.249853608928,26.7589720791278,-72.0137743378471));
#7893=CARTESIAN_POINT('Ctrl Pts',(-23.2535066048616,26.759312062963,-72.0135463948183));
#7894=CARTESIAN_POINT('Ctrl Pts',(-23.2554110765952,26.7594876020332,-72.0134276652749));
#7895=CARTESIAN_POINT('Ctrl Pts',(-23.2599535901904,26.7599022171677,-72.0131447275792));
#7896=CARTESIAN_POINT('Ctrl Pts',(-23.2625917805339,26.760139737074,-72.0129806079157));
#7897=CARTESIAN_POINT('Ctrl Pts',(-23.2714752004608,26.7609284836812,-72.0124286561463));
#7898=CARTESIAN_POINT('Ctrl Pts',(-23.2777217956614,26.7614647433921,-72.0120416665226));
#7899=CARTESIAN_POINT('Ctrl Pts',(-23.3991177989233,26.7715296103938,-72.004542168137));
#7900=CARTESIAN_POINT('Ctrl Pts',(-23.5147110585094,26.774878304985,-71.9977714576884));
#7901=CARTESIAN_POINT('Ctrl Pts',(-23.6619362323438,26.7712227391739,-71.9893401023769));
#7902=CARTESIAN_POINT('Ctrl Pts',(-23.6936117462741,26.7699684410239,-71.9875375207124));
#7903=CARTESIAN_POINT('Ctrl Pts',(-23.7507387905546,26.7668615689717,-71.9842994866458));
#7904=CARTESIAN_POINT('Ctrl Pts',(-23.7761963407392,26.7651736599611,-71.9828611684297));
#7905=CARTESIAN_POINT('Ctrl Pts',(-23.8230122160864,26.7615107981696,-71.9802207439004));
#7906=CARTESIAN_POINT('Ctrl Pts',(-23.8443759112048,26.7596245805155,-71.9790176000795));
#7907=CARTESIAN_POINT('Ctrl Pts',(-23.8840844495161,26.7557188557649,-71.9767823330282));
#7908=CARTESIAN_POINT('Ctrl Pts',(-23.9024337955236,26.7537547504446,-71.9757498161742));
#7909=CARTESIAN_POINT('Ctrl Pts',(-24.0741360247475,26.7338827396877,-71.9660847826646));
#7910=CARTESIAN_POINT('Ctrl Pts',(-24.2260293219561,26.7051341908807,-71.9574980327719));
#7911=CARTESIAN_POINT('Ctrl Pts',(-24.419680021313,26.6538510737702,-71.9460232244059));
#7912=CARTESIAN_POINT('Ctrl Pts',(-24.4638315080081,26.641142578506,-71.9433713650675));
#7913=CARTESIAN_POINT('Ctrl Pts',(-24.5990746592239,26.5990634957281,-71.9351157939515));
#7914=CARTESIAN_POINT('Ctrl Pts',(-24.6891345360214,26.5665783039343,-71.9294289240575));
#7915=CARTESIAN_POINT('Ctrl Pts',(-24.787013245412,26.5262639441243,-71.9229853546441));
#7916=CARTESIAN_POINT('Ctrl Pts',(-24.7963982974406,26.5223463587285,-71.9223648068401));
#7917=CARTESIAN_POINT('Ctrl Pts',(-24.8096116433367,26.5167571479975,-71.921487246525));
#7918=CARTESIAN_POINT('Ctrl Pts',(-24.8134555393248,26.5151223723232,-71.9212314901779));
#7919=CARTESIAN_POINT('Ctrl Pts',(-24.8201725713095,26.512250242943,-71.920783749227));
#7920=CARTESIAN_POINT('Ctrl Pts',(-24.8230471107394,26.5110161676348,-71.9205918767531));
#7921=CARTESIAN_POINT('Ctrl Pts',(-24.8288376943503,26.5085202072138,-71.9202048295779));
#7922=CARTESIAN_POINT('Ctrl Pts',(-24.8317536776283,26.5072581913176,-71.9200096505886));
#7923=CARTESIAN_POINT('Ctrl Pts',(-24.8377393819307,26.504657106103,-71.9196084404333));
#7924=CARTESIAN_POINT('Ctrl Pts',(-24.8408088903945,26.5033175603893,-71.9194023931283));
#7925=CARTESIAN_POINT('Ctrl Pts',(-24.8511054186184,26.498804994692,-71.9187101914128));
#7926=CARTESIAN_POINT('Ctrl Pts',(-24.858322825577,26.4956102289789,-71.9182232911356));
#7927=CARTESIAN_POINT('Ctrl Pts',(-24.9109190236838,26.4720972106927,-71.9146625352952));
#7928=CARTESIAN_POINT('Ctrl Pts',(-24.955831813811,26.4507587057636,-71.9115536421922));
#7929=CARTESIAN_POINT('Ctrl Pts',(-25.1002455404749,26.3780044486529,-71.9013250673531));
#7930=CARTESIAN_POINT('Ctrl Pts',(-25.1975550860571,26.3224445933505,-71.8940630623985));
#7931=CARTESIAN_POINT('Ctrl Pts',(-25.3358341005038,26.2336382275399,-71.8831998233624));
#7932=CARTESIAN_POINT('Ctrl Pts',(-25.3792026372575,26.2042686394421,-71.879709780857));
#7933=CARTESIAN_POINT('Ctrl Pts',(-25.655000731967,26.0075244217124,-71.8570000669935));
#7934=CARTESIAN_POINT('Ctrl Pts',(-25.8649558794357,25.8108521435721,-71.8371523588841));
#7935=CARTESIAN_POINT('Ctrl Pts',(-26.0469270226487,25.5880787073612,-71.8189541869717));
#7936=CARTESIAN_POINT('Ctrl Pts',(-26.0476944169045,25.5871381607917,-71.8188774246931));
#7937=CARTESIAN_POINT('Ctrl Pts',(-26.0502162651769,25.5840437233147,-71.8186251048704));
#7938=CARTESIAN_POINT('Ctrl Pts',(-26.0519684715928,25.5818879901434,-71.8184496949777));
#7939=CARTESIAN_POINT('Ctrl Pts',(-26.0615588713071,25.5700577362658,-71.8174891077348));
#7940=CARTESIAN_POINT('Ctrl Pts',(-26.0693438804661,25.5603399388437,-71.8167074735066));
#7941=CARTESIAN_POINT('Ctrl Pts',(-26.0793125842562,25.5477474222682,-71.815704422678));
#7942=CARTESIAN_POINT('Ctrl Pts',(-26.0815479041501,25.5449139879374,-71.8154793625923));
#7943=CARTESIAN_POINT('Ctrl Pts',(-26.0849578017679,25.5405767257302,-71.8151358317497));
#7944=CARTESIAN_POINT('Ctrl Pts',(-26.0861358018862,25.539075611686,-71.815017115397));
#7945=CARTESIAN_POINT('Ctrl Pts',(-26.0883467293317,25.536253090468,-71.8147942318552));
#7946=CARTESIAN_POINT('Ctrl Pts',(-26.0893799542326,25.5349319283924,-71.8146900434126));
#7947=CARTESIAN_POINT('Ctrl Pts',(-26.0917554631376,25.531889525773,-71.814450434498));
#7948=CARTESIAN_POINT('Ctrl Pts',(-26.0930970277136,25.5301677308804,-71.8143150660899));
#7949=CARTESIAN_POINT('Ctrl Pts',(-26.096826370712,25.5253713633959,-71.8139386201053));
#7950=CARTESIAN_POINT('Ctrl Pts',(-26.0992103392914,25.5222938122918,-71.8136978151944));
#7951=CARTESIAN_POINT('Ctrl Pts',(-26.1124755446422,25.5051050379774,-71.8123569355295));
#7952=CARTESIAN_POINT('Ctrl Pts',(-26.1232454555291,25.4909077142549,-71.8112646718845));
#7953=CARTESIAN_POINT('Ctrl Pts',(-26.2973028190546,25.2574620802049,-71.7935390696248));
#7954=CARTESIAN_POINT('Ctrl Pts',(-26.4321889122551,25.018362273839,-71.778674267329));
#7955=CARTESIAN_POINT('Ctrl Pts',(-26.5569493949703,24.7118024759663,-71.7601002042237));
#7956=CARTESIAN_POINT('Ctrl Pts',(-26.5771956499849,24.657970630244,-71.7568587218997));
#7957=CARTESIAN_POINT('Ctrl Pts',(-26.6023819104174,24.5851468206001,-71.7524763406382));
#7958=CARTESIAN_POINT('Ctrl Pts',(-26.6086049571469,24.5666089455675,-71.7513610267112));
#7959=CARTESIAN_POINT('Ctrl Pts',(-26.6589273087568,24.4120551132626,-71.7420593635531));
#7960=CARTESIAN_POINT('Ctrl Pts',(-26.6940930097462,24.2733163970913,-71.7336795079067));
#7961=CARTESIAN_POINT('Ctrl Pts',(-26.7219339810059,24.1218094058783,-71.7243092318042));
#7962=CARTESIAN_POINT('Ctrl Pts',(-26.723881417089,24.1108951712689,-71.7236330734398));
#7963=CARTESIAN_POINT('Ctrl Pts',(-26.7265186365875,24.0956609370378,-71.7226876203253));
#7964=CARTESIAN_POINT('Ctrl Pts',(-26.7272560146339,24.0913491652035,-71.7224198417323));
#7965=CARTESIAN_POINT('Ctrl Pts',(-26.728514000102,24.083901951222,-71.7219570146538));
#7966=CARTESIAN_POINT('Ctrl Pts',(-26.7290387534146,24.0807672072871,-71.7217620983237));
#7967=CARTESIAN_POINT('Ctrl Pts',(-26.7301150540854,24.0742787266205,-71.7213584413241));
#7968=CARTESIAN_POINT('Ctrl Pts',(-26.7306659347774,24.0709248851257,-71.7211496797484));
#7969=CARTESIAN_POINT('Ctrl Pts',(-26.7317467873486,24.0642787796954,-71.7207357600284));
#7970=CARTESIAN_POINT('Ctrl Pts',(-26.7322769569193,24.0609865520355,-71.720530608472));
#7971=CARTESIAN_POINT('Ctrl Pts',(-26.7334935356628,24.0533564587628,-71.7200548867378));
#7972=CARTESIAN_POINT('Ctrl Pts',(-26.7341761880694,24.0490180084929,-71.7197841974273));
#7973=CARTESIAN_POINT('Ctrl Pts',(-26.7359198412538,24.0377871321686,-71.719082956958));
#7974=CARTESIAN_POINT('Ctrl Pts',(-26.7369673384183,24.0308926603085,-71.7186519774751));
#7975=CARTESIAN_POINT('Ctrl Pts',(-26.7614327531121,23.8662686233218,-71.7083490817075));
#7976=CARTESIAN_POINT('Ctrl Pts',(-26.7731304536971,23.7070502666355,-71.6981022652118));
#7977=CARTESIAN_POINT('Ctrl Pts',(-26.7730014767856,23.5476449634564,-71.6875616724776));
#7978=CARTESIAN_POINT('Ctrl Pts',(-26.7730014799568,23.547648885711,-71.6875619318346));
#7979=CARTESIAN_POINT('Ctrl Pts',(-26.7727984241538,23.2963098481987,-71.6709422755845));
#7980=CARTESIAN_POINT('Ctrl Pts',(-26.7431956845923,23.0458728685053,-71.6536303384008));
#7981=CARTESIAN_POINT('Ctrl Pts',(-26.6681982469996,22.7319401547143,-71.6322143859523));
#7982=CARTESIAN_POINT('Ctrl Pts',(-26.6492926480794,22.6630250719862,-71.627538329957));
#7983=CARTESIAN_POINT('Ctrl Pts',(-26.6193024310339,22.5664167070907,-71.6210710084051));
#7984=CARTESIAN_POINT('Ctrl Pts',(-26.6101020192241,22.5381648459333,-71.6191906070202));
#7985=CARTESIAN_POINT('Ctrl Pts',(-26.599060805269,22.5057881315206,-71.6170514996445));
#7986=CARTESIAN_POINT('Ctrl Pts',(-26.597600869188,22.501536229348,-71.6167708959201));
#7987=CARTESIAN_POINT('Ctrl Pts',(-26.595376660822,22.4951023311725,-71.6163467864058));
#7988=CARTESIAN_POINT('Ctrl Pts',(-26.5946189373499,22.4929181022667,-71.6162028929383));
#7989=CARTESIAN_POINT('Ctrl Pts',(-26.5933041211787,22.4891411174585,-71.6159542232738));
#7990=CARTESIAN_POINT('Ctrl Pts',(-26.5927481289417,22.4875479864589,-71.6158493813996));
#7991=CARTESIAN_POINT('Ctrl Pts',(-26.5915863812581,22.4842275185812,-71.6156309639871));
#7992=CARTESIAN_POINT('Ctrl Pts',(-26.5909804070489,22.4825002658729,-71.6155174021068));
#7993=CARTESIAN_POINT('Ctrl Pts',(-26.5893032493548,22.4777327469817,-71.6152041016831));
#7994=CARTESIAN_POINT('Ctrl Pts',(-26.5882289718043,22.4746935595009,-71.6150045483498));
#7995=CARTESIAN_POINT('Ctrl Pts',(-26.5840140606707,22.462826051303,-71.6142259673887));
#7996=CARTESIAN_POINT('Ctrl Pts',(-26.5808394496311,22.4540097196656,-71.6136489487729));
#7997=CARTESIAN_POINT('Ctrl Pts',(-26.52321221848,22.2961345875922,-71.6033389873893));
#7998=CARTESIAN_POINT('Ctrl Pts',(-26.4578527497856,22.1512610321307,-71.5942386101509));
#7999=CARTESIAN_POINT('Ctrl Pts',(-26.2988864532468,21.8586573009056,-71.5754732371789));
#8000=CARTESIAN_POINT('Ctrl Pts',(-26.2034192503403,21.7125393552298,-71.565862302377));
#8001=CARTESIAN_POINT('Ctrl Pts',(-26.055900040713,21.5223820710765,-71.552204431212));
#8002=CARTESIAN_POINT('Ctrl Pts',(-26.013582252558,21.4711820473899,-71.5484008779054));
#8003=CARTESIAN_POINT('Ctrl Pts',(-25.899880438966,21.3419631961191,-71.5384064354533));
#8004=CARTESIAN_POINT('Ctrl Pts',(-25.8261903774889,21.2660904644569,-71.5321394105468));
#8005=CARTESIAN_POINT('Ctrl Pts',(-25.7417847705233,21.1873308195238,-71.5251098668673));
#8006=CARTESIAN_POINT('Ctrl Pts',(-25.7346281143957,21.1807133608662,-71.5245149715753));
#8007=CARTESIAN_POINT('Ctrl Pts',(-25.7248203790968,21.1717267532111,-71.5237011990923));
#8008=CARTESIAN_POINT('Ctrl Pts',(-25.7221951849842,21.1693293257665,-71.5234835251041));
#8009=CARTESIAN_POINT('Ctrl Pts',(-25.7172494851197,21.164827710259,-71.5230737105314));
#8010=CARTESIAN_POINT('Ctrl Pts',(-25.7149298662775,21.1627225503315,-71.5228816114488));
#8011=CARTESIAN_POINT('Ctrl Pts',(-25.7100910198412,21.1583439249956,-71.5224811116568));
#8012=CARTESIAN_POINT('Ctrl Pts',(-25.7075712644598,21.1560710509375,-71.5222726863114));
#8013=CARTESIAN_POINT('Ctrl Pts',(-25.7017530158239,21.1508395069903,-71.5217917148934));
#8014=CARTESIAN_POINT('Ctrl Pts',(-25.698452006636,21.1478836566304,-71.5215190505276));
#8015=CARTESIAN_POINT('Ctrl Pts',(-25.6881603380773,21.1387062744476,-71.520669621159));
#8016=CARTESIAN_POINT('Ctrl Pts',(-25.6811487151363,21.1325084195389,-71.5200918645438));
#8017=CARTESIAN_POINT('Ctrl Pts',(-25.6214473146192,21.0801973959269,-71.5151803290809));
#8018=CARTESIAN_POINT('Ctrl Pts',(-25.5672982318415,21.0357852712132,-71.5107765591166));
#8019=CARTESIAN_POINT('Ctrl Pts',(-25.5049638050972,20.9879694616461,-71.5057568606334));
#8020=CARTESIAN_POINT('Ctrl Pts',(-25.4981578842387,20.9827916403157,-71.5052094443436));
#8021=CARTESIAN_POINT('Ctrl Pts',(-25.4492876799623,20.9459182437194,-71.5012833568309));
#8022=CARTESIAN_POINT('Ctrl Pts',(-25.4064744990272,20.9152323987471,-71.4978682822105));
#8023=CARTESIAN_POINT('Ctrl Pts',(-25.2931513295494,20.8381419609986,-71.4888939404068));
#8024=CARTESIAN_POINT('Ctrl Pts',(-25.221538666748,20.7934353333824,-71.4832851113866));
#8025=CARTESIAN_POINT('Ctrl Pts',(-25.094022835964,20.7206251243107,-71.4734337360726));
#8026=CARTESIAN_POINT('Ctrl Pts',(-25.0389000355938,20.6912411083891,-71.469217309668));
#8027=CARTESIAN_POINT('Ctrl Pts',(-24.8700820920327,20.6074567249871,-71.4564670264848));
#8028=CARTESIAN_POINT('Ctrl Pts',(-24.754012921954,20.5581027945711,-71.4479132654968));
#8029=CARTESIAN_POINT('Ctrl Pts',(-24.563828650898,20.4900972740889,-71.4344764452376));
#8030=CARTESIAN_POINT('Ctrl Pts',(-24.4914206595373,20.4670575769851,-71.4294904243623));
#8031=CARTESIAN_POINT('Ctrl Pts',(-24.3870860164065,20.4378780097799,-71.4225508819997));
#8032=CARTESIAN_POINT('Ctrl Pts',(-24.3557801331197,20.4296290476998,-71.4204995956354));
#8033=CARTESIAN_POINT('Ctrl Pts',(-24.3198979855948,20.4207502537141,-71.4181878090742));
#8034=CARTESIAN_POINT('Ctrl Pts',(-24.3154397697522,20.4196572011016,-71.4179012691486));
#8035=CARTESIAN_POINT('Ctrl Pts',(-24.3087135251834,20.4180233063594,-71.4174700143657));
#8036=CARTESIAN_POINT('Ctrl Pts',(-24.306447244181,20.4174754002059,-71.4173248919046));
#8037=CARTESIAN_POINT('Ctrl Pts',(-24.3025374699571,20.4165346456164,-71.4170748414792));
#8038=CARTESIAN_POINT('Ctrl Pts',(-24.300894264491,20.4161406308689,-71.4169698456022));
#8039=CARTESIAN_POINT('Ctrl Pts',(-24.2974791876764,20.4153245891924,-71.4167518317465));
#8040=CARTESIAN_POINT('Ctrl Pts',(-24.2957072731602,20.4149027731259,-71.4166388263206));
#8041=CARTESIAN_POINT('Ctrl Pts',(-24.2908424197197,20.413749019466,-71.4163288687149));
#8042=CARTESIAN_POINT('Ctrl Pts',(-24.2877487434761,20.4130201523063,-71.4161320950558));
#8043=CARTESIAN_POINT('Ctrl Pts',(-24.2758450337367,20.410234230586,-71.4153762314205));
#8044=CARTESIAN_POINT('Ctrl Pts',(-24.2670273225602,20.408209674869,-71.4148190041085));
#8045=CARTESIAN_POINT('Ctrl Pts',(-24.2502457691316,20.4044309337968,-71.4137633990485));
#8046=CARTESIAN_POINT('Ctrl Pts',(-24.2422835929154,20.4026697969918,-71.4132646440288));
#8047=CARTESIAN_POINT('Ctrl Pts',(-23.9551854363941,20.3403092272776,-71.3953529886996));
#8048=CARTESIAN_POINT('Ctrl Pts',(-23.6691823992768,20.3170461829979,-71.379892110277));
#8049=CARTESIAN_POINT('Ctrl Pts',(-23.2700704773358,20.337685193692,-71.3574244618303));
#8050=CARTESIAN_POINT('Ctrl Pts',(-23.156720518798,20.3495931256951,-71.3509539521676));
#8051=CARTESIAN_POINT('Ctrl Pts',(-22.9779959448537,20.3780072983004,-71.3404130508502));
#8052=CARTESIAN_POINT('Ctrl Pts',(-22.9120957354779,20.3906050194246,-71.336452737286));
#8053=CARTESIAN_POINT('Ctrl Pts',(-22.8123525809333,20.4129199581823,-71.330319653314));
#8054=CARTESIAN_POINT('Ctrl Pts',(-22.7781942493942,20.4211507639194,-71.3281942098128));
#8055=CARTESIAN_POINT('Ctrl Pts',(-22.7372362328648,20.4317314929742,-71.325613194918));
#8056=CARTESIAN_POINT('Ctrl Pts',(-22.7303002014443,20.4335479987126,-71.3251749868323));
#8057=CARTESIAN_POINT('Ctrl Pts',(-22.720206236866,20.436227575473,-71.3245356046553));
#8058=CARTESIAN_POINT('Ctrl Pts',(-22.7170434311509,20.4370723451048,-71.3243350251251));
#8059=CARTESIAN_POINT('Ctrl Pts',(-22.7107579079904,20.43876144163,-71.3239359329842));
#8060=CARTESIAN_POINT('Ctrl Pts',(-22.7076351635345,20.439605654029,-71.3237374242975));
#8061=CARTESIAN_POINT('Ctrl Pts',(-22.701410858797,20.4412984122862,-71.323341285468));
#8062=CARTESIAN_POINT('Ctrl Pts',(-22.6983092866325,20.4421469013627,-71.3231436573608));
#8063=CARTESIAN_POINT('Ctrl Pts',(-22.6908566217321,20.4441977011988,-71.3226682228132));
#8064=CARTESIAN_POINT('Ctrl Pts',(-22.6865067835128,20.4454045125023,-71.32239026993));
#8065=CARTESIAN_POINT('Ctrl Pts',(-22.6732007508227,20.4491262404023,-71.3215386035544));
#8066=CARTESIAN_POINT('Ctrl Pts',(-22.6642529573395,20.4516707831839,-71.3209639243285));
#8067=CARTESIAN_POINT('Ctrl Pts',(-22.5622749512569,20.4811487701997,-71.3143915861999));
#8068=CARTESIAN_POINT('Ctrl Pts',(-22.470502308384,20.512221294842,-71.3082585695236));
#8069=CARTESIAN_POINT('Ctrl Pts',(-22.2302128276252,20.6058426057763,-71.2915856277272));
#8070=CARTESIAN_POINT('Ctrl Pts',(-22.0847613751605,20.6754691791696,-71.2808326711107));
#8071=CARTESIAN_POINT('Ctrl Pts',(-21.842904345346,20.8143835122696,-71.2619923361145));
#8072=CARTESIAN_POINT('Ctrl Pts',(-21.7439696744951,20.8786687471491,-71.253980748827));
#8073=CARTESIAN_POINT('Ctrl Pts',(-21.5887249086116,20.9921166045432,-71.2410860709034));
#8074=CARTESIAN_POINT('Ctrl Pts',(-21.5302040987066,21.0380710655074,-71.2361444842696));
#8075=CARTESIAN_POINT('Ctrl Pts',(-21.4467037075505,21.1084474967784,-71.229028669011));
#8076=CARTESIAN_POINT('Ctrl Pts',(-21.4204486643998,21.1313136767297,-71.2267813694454));
#8077=CARTESIAN_POINT('Ctrl Pts',(-21.3747975354672,21.1723920449945,-71.2228639343417));
#8078=CARTESIAN_POINT('Ctrl Pts',(-21.3552470743839,21.1904270953873,-71.2211829348023));
#8079=CARTESIAN_POINT('Ctrl Pts',(-21.3327462100764,21.2117054670375,-71.2192466975512));
#8080=CARTESIAN_POINT('Ctrl Pts',(-21.3295771402601,21.2147145922794,-71.2189739574236));
#8081=CARTESIAN_POINT('Ctrl Pts',(-21.3247599270849,21.2193073471502,-71.2185593313556));
#8082=CARTESIAN_POINT('Ctrl Pts',(-21.3231073475098,21.2208862841579,-71.218417083432));
#8083=CARTESIAN_POINT('Ctrl Pts',(-21.3201096770173,21.223756478225,-71.2181590438643));
#8084=CARTESIAN_POINT('Ctrl Pts',(-21.3187640315217,21.2250471401804,-71.2180432067232));
#8085=CARTESIAN_POINT('Ctrl Pts',(-21.3158489014319,21.2278480183647,-71.2177922552897));
#8086=CARTESIAN_POINT('Ctrl Pts',(-21.3142798318529,21.2293586538758,-71.2176571749946));
#8087=CARTESIAN_POINT('Ctrl Pts',(-21.309999399835,21.2334880471154,-71.2172886556549));
#8088=CARTESIAN_POINT('Ctrl Pts',(-21.3072910877586,21.2361099835408,-71.2170554650276));
#8089=CARTESIAN_POINT('Ctrl Pts',(-21.2942525822178,21.2487770468914,-71.2159326856354));
#8090=CARTESIAN_POINT('Ctrl Pts',(-21.2839850225099,21.2588868309988,-71.2150480940606));
#8091=CARTESIAN_POINT('Ctrl Pts',(-21.0988731909654,21.4436156457803,-71.1990843658078));
#8092=CARTESIAN_POINT('Ctrl Pts',(-20.9445847888198,21.6377362862193,-71.18548517627));
#8093=CARTESIAN_POINT('Ctrl Pts',(-20.7284409129194,21.9850957923487,-71.1626057088043));
#8094=CARTESIAN_POINT('Ctrl Pts',(-20.6533826083418,22.1288184913387,-71.1534942610463));
#8095=CARTESIAN_POINT('Ctrl Pts',(-20.565146364387,22.3340926259622,-71.1404365913821));
#8096=CARTESIAN_POINT('Ctrl Pts',(-20.5424721427305,22.3913046669938,-71.1367947596021));
#8097=CARTESIAN_POINT('Ctrl Pts',(-20.5140720707222,22.4694231732193,-71.1318013206306));
#8098=CARTESIAN_POINT('Ctrl Pts',(-20.5068980731353,22.4897915476394,-71.1304975092768));
#8099=CARTESIAN_POINT('Ctrl Pts',(-20.4967318216469,22.51960855061,-71.1285855794885));
#8100=CARTESIAN_POINT('Ctrl Pts',(-20.4935774945517,22.5290016044873,-71.1279828035802));
#8101=CARTESIAN_POINT('Ctrl Pts',(-20.4880016727925,22.545862729971,-71.1268998701347));
#8102=CARTESIAN_POINT('Ctrl Pts',(-20.4855640453356,22.5533254147435,-71.1264202478617));
#8103=CARTESIAN_POINT('Ctrl Pts',(-20.4818984404577,22.564687998122,-71.1256894710931));
#8104=CARTESIAN_POINT('Ctrl Pts',(-20.4806505642224,22.5685814869489,-71.1254389731326));
#8105=CARTESIAN_POINT('Ctrl Pts',(-20.4784899217689,22.5753672925966,-71.1250022281297));
#8106=CARTESIAN_POINT('Ctrl Pts',(-20.4775738210406,22.5782585491309,-71.1248160911702));
#8107=CARTESIAN_POINT('Ctrl Pts',(-20.4756873161201,22.5842417659109,-71.1244307884116));
#8108=CARTESIAN_POINT('Ctrl Pts',(-20.4747174918361,22.5873339043414,-71.1242316037641));
#8109=CARTESIAN_POINT('Ctrl Pts',(-20.4723803678538,22.5948250220788,-71.1237489060589));
#8110=CARTESIAN_POINT('Ctrl Pts',(-20.4710178356089,22.5992254715348,-71.1234652366147));
#8111=CARTESIAN_POINT('Ctrl Pts',(-20.4659886315635,22.6155919582176,-71.1224097274929));
#8112=CARTESIAN_POINT('Ctrl Pts',(-20.4623822749201,22.6275762810566,-71.1216359116738));
#8113=CARTESIAN_POINT('Ctrl Pts',(-20.3844452515622,22.8921448673834,-71.1045315440814));
#8114=CARTESIAN_POINT('Ctrl Pts',(-20.3412922154416,23.1528162505785,-71.0871228470884));
#8115=CARTESIAN_POINT('Ctrl Pts',(-20.3240132394544,23.566524795566,-71.0591301289729));
#8116=CARTESIAN_POINT('Ctrl Pts',(-20.3283117974109,23.7175421312417,-71.0488664585046));
#8117=CARTESIAN_POINT('Ctrl Pts',(-20.3510489148938,23.9472435580378,-71.0335930866709));
#8118=CARTESIAN_POINT('Ctrl Pts',(-20.3618787915508,24.0264677505785,-71.0283900120778));
#8119=CARTESIAN_POINT('Ctrl Pts',(-20.3783070472814,24.1204441221017,-71.022357914383));
#8120=CARTESIAN_POINT('Ctrl Pts',(-20.3810790834573,24.135655199711,-71.0213859833258));
#8121=CARTESIAN_POINT('Ctrl Pts',(-20.3846535423618,24.1544995250735,-71.0201879002099));
#8122=CARTESIAN_POINT('Ctrl Pts',(-20.3853528643272,24.1581517717847,-71.019955978049));
#8123=CARTESIAN_POINT('Ctrl Pts',(-20.3864653970981,24.1639080760484,-71.0195908963074));
#8124=CARTESIAN_POINT('Ctrl Pts',(-20.3868743863002,24.166012931087,-71.0194574952819));
#8125=CARTESIAN_POINT('Ctrl Pts',(-20.3876434873805,24.1699501050022,-71.019208145893));
#8126=CARTESIAN_POINT('Ctrl Pts',(-20.3880030886792,24.1717825066078,-71.0190921692937));
#8127=CARTESIAN_POINT('Ctrl Pts',(-20.3888149142104,24.1759003406818,-71.0188317064623));
#8128=CARTESIAN_POINT('Ctrl Pts',(-20.3892680231688,24.1781855910955,-71.0186872720412));
#8129=CARTESIAN_POINT('Ctrl Pts',(-20.3904277157938,24.1840014248066,-71.018319977942));
#8130=CARTESIAN_POINT('Ctrl Pts',(-20.3911377410017,24.1875313295665,-71.0180973157263));
#8131=CARTESIAN_POINT('Ctrl Pts',(-20.3951123601556,24.2071213500731,-71.0168630401017));
#8132=CARTESIAN_POINT('Ctrl Pts',(-20.3984935835882,24.22315795329,-71.015858022988));
#8133=CARTESIAN_POINT('Ctrl Pts',(-20.46953507487,24.5478082514731,-70.9956084201467));
#8134=CARTESIAN_POINT('Ctrl Pts',(-20.5821030396575,24.8448970158884,-70.9787187806519));
#8135=CARTESIAN_POINT('Ctrl Pts',(-20.8219996512642,25.2747206437379,-70.9508521107429));
#8136=CARTESIAN_POINT('Ctrl Pts',(-20.9203144205121,25.4212324546322,-70.9406426832417));
#8137=CARTESIAN_POINT('Ctrl Pts',(-21.0356934351114,25.5659883138695,-70.9293974600802));
#8138=CARTESIAN_POINT('Ctrl Pts',(-21.0413195566681,25.5729867005915,-70.9288508125927));
#8139=CARTESIAN_POINT('Ctrl Pts',(-21.0515334744962,25.5855837153704,-70.9278613969213));
#8140=CARTESIAN_POINT('Ctrl Pts',(-21.0561110389804,25.5911905922497,-70.9274190425282));
#8141=CARTESIAN_POINT('Ctrl Pts',(-21.0632207975736,25.5998394122654,-70.9267336186967));
#8142=CARTESIAN_POINT('Ctrl Pts',(-21.0657397923273,25.6028922164009,-70.9264910861314));
#8143=CARTESIAN_POINT('Ctrl Pts',(-21.0701892571456,25.6082643934071,-70.9260632332505));
#8144=CARTESIAN_POINT('Ctrl Pts',(-21.0721173768674,25.6105857142233,-70.9258780089972));
#8145=CARTESIAN_POINT('Ctrl Pts',(-21.0764712056878,25.615812465277,-70.9254601637691));
#8146=CARTESIAN_POINT('Ctrl Pts',(-21.0788987753781,25.6187163334243,-70.925227466793));
#8147=CARTESIAN_POINT('Ctrl Pts',(-21.0854288713786,25.6264997536985,-70.9246022678674));
#8148=CARTESIAN_POINT('Ctrl Pts',(-21.0895407545164,25.631371401931,-70.9242093819337));
#8149=CARTESIAN_POINT('Ctrl Pts',(-21.1075288868192,25.6525554121828,-70.9224940366049));
#8150=CARTESIAN_POINT('Ctrl Pts',(-21.1215528310653,25.6687411285581,-70.921165484296));
#8151=CARTESIAN_POINT('Ctrl Pts',(-21.3681760257171,25.947713427733,-70.8979482160917));
#8152=CARTESIAN_POINT('Ctrl Pts',(-21.6419634531248,26.1708587526071,-70.8740219971911));
#8153=CARTESIAN_POINT('Ctrl Pts',(-21.9886033311619,26.3697847092624,-70.847154366132));
#8154=CARTESIAN_POINT('Ctrl Pts',(-22.0315665040648,26.3931561195988,-70.8438841383696));
#8155=CARTESIAN_POINT('Ctrl Pts',(-22.0750360699906,26.4155368026905,-70.8406447795461));
#8156=CARTESIAN_POINT('Origin',(-23.5502525316942,23.5502525316942,-77.3107734492734));
#8157=CARTESIAN_POINT('',(-22.075036015343,26.4155367745547,-69.3432196869019));
#8158=CARTESIAN_POINT('',(-22.0750360905742,26.4155368132881,-69.5918437005959));
#8159=CARTESIAN_POINT('',(-22.0750360153461,26.4155367745563,-77.3107734492734));
#8160=CARTESIAN_POINT('Ctrl Pts',(-22.075036015343,26.4155367745547,-69.3432196869019));
#8161=CARTESIAN_POINT('Ctrl Pts',(-22.0700252443756,26.4129569355355,-69.3435677364703));
#8162=CARTESIAN_POINT('Ctrl Pts',(-22.0650212677462,26.4103639662412,-69.3439162512079));
#8163=CARTESIAN_POINT('Ctrl Pts',(-21.9680557316067,26.3597951038903,-69.3506879650293));
#8164=CARTESIAN_POINT('Ctrl Pts',(-21.878466134713,26.3074254374581,-69.3572675485728));
#8165=CARTESIAN_POINT('Ctrl Pts',(-21.6267416012296,26.1434958781456,-69.3767445377577));
#8166=CARTESIAN_POINT('Ctrl Pts',(-21.4721100761709,26.0213072430003,-69.3900039017954));
#8167=CARTESIAN_POINT('Ctrl Pts',(-21.3061862398938,25.8635462252343,-69.405502002912));
#8168=CARTESIAN_POINT('Ctrl Pts',(-21.2831098195613,25.8409347825109,-69.4076884173614));
#8169=CARTESIAN_POINT('Ctrl Pts',(-21.2339943888438,25.791339666148,-69.412404608083));
#8170=CARTESIAN_POINT('Ctrl Pts',(-21.2080781314018,25.7642404461029,-69.4149328203265));
#8171=CARTESIAN_POINT('Ctrl Pts',(-21.1460260538257,25.6970466958991,-69.4210743582906));
#8172=CARTESIAN_POINT('Ctrl Pts',(-21.1104120494764,25.6564835275016,-69.4246755728561));
#8173=CARTESIAN_POINT('Ctrl Pts',(-21.029200840972,25.5591610152318,-69.4330382830035));
#8174=CARTESIAN_POINT('Ctrl Pts',(-20.9844716028786,25.5017096785125,-69.4377646379455));
#8175=CARTESIAN_POINT('Ctrl Pts',(-20.9326047720579,25.430220312707,-69.4433494679472));
#8176=CARTESIAN_POINT('Ctrl Pts',(-20.9235773655829,25.4175865259414,-69.4443255817774));
#8177=CARTESIAN_POINT('Ctrl Pts',(-20.9124984979293,25.4018424122081,-69.4455281163117));
#8178=CARTESIAN_POINT('Ctrl Pts',(-20.9103608552575,25.3987934063515,-69.4457603582092));
#8179=CARTESIAN_POINT('Ctrl Pts',(-20.9070000114916,25.3939819801598,-69.446125825153));
#8180=CARTESIAN_POINT('Ctrl Pts',(-20.9057732859736,25.3922220438508,-69.4462592925129));
#8181=CARTESIAN_POINT('Ctrl Pts',(-20.9034821741442,25.3889280667083,-69.4465086938957));
#8182=CARTESIAN_POINT('Ctrl Pts',(-20.9024173708622,25.3873943361701,-69.4466246563016));
#8183=CARTESIAN_POINT('Ctrl Pts',(-20.9000279466759,25.3839462440655,-69.446884994697));
#8184=CARTESIAN_POINT('Ctrl Pts',(-20.8987040696066,25.3820313761837,-69.4470293190714));
#8185=CARTESIAN_POINT('Ctrl Pts',(-20.8953410000555,25.3771557163729,-69.4473961627538));
#8186=CARTESIAN_POINT('Ctrl Pts',(-20.8933046787734,25.3741929348225,-69.4476184854174));
#8187=CARTESIAN_POINT('Ctrl Pts',(-20.8820514033343,25.3577609471945,-69.4488482537072));
#8188=CARTESIAN_POINT('Ctrl Pts',(-20.8729316942325,25.3442249654902,-69.4498491588648));
#8189=CARTESIAN_POINT('Ctrl Pts',(-20.6877069337447,25.064745447452,-69.4702800259876));
#8190=CARTESIAN_POINT('Ctrl Pts',(-20.5519118916773,24.7741356094699,-69.4873108809933));
#8191=CARTESIAN_POINT('Ctrl Pts',(-20.424811613949,24.3464259833338,-69.5125905978506));
#8192=CARTESIAN_POINT('Ctrl Pts',(-20.3958483442435,24.2225637549597,-69.51991432577));
#8193=CARTESIAN_POINT('Ctrl Pts',(-20.3682584012077,24.0623924313075,-69.5295769490699));
#8194=CARTESIAN_POINT('Ctrl Pts',(-20.3628183554681,24.0273658798772,-69.5317010815362));
#8195=CARTESIAN_POINT('Ctrl Pts',(-20.3559923275292,23.9780662411099,-69.5347092823438));
#8196=CARTESIAN_POINT('Ctrl Pts',(-20.3541220542966,23.9638619888815,-69.5355781495236));
#8197=CARTESIAN_POINT('Ctrl Pts',(-20.3514397191732,23.942384779046,-69.5368953091249));
#8198=CARTESIAN_POINT('Ctrl Pts',(-20.3505575995965,23.935120624791,-69.5373413949648));
#8199=CARTESIAN_POINT('Ctrl Pts',(-20.3491687249311,23.9233485016198,-69.5380652866643));
#8200=CARTESIAN_POINT('Ctrl Pts',(-20.3486467311437,23.9188423284133,-69.5383426116148));
#8201=CARTESIAN_POINT('Ctrl Pts',(-20.3476638567574,23.9101979152248,-69.5388750672006));
#8202=CARTESIAN_POINT('Ctrl Pts',(-20.3472014783216,23.9060598520076,-69.5391301500468));
#8203=CARTESIAN_POINT('Ctrl Pts',(-20.3463875023282,23.8986449788287,-69.5395875833411));
#8204=CARTESIAN_POINT('Ctrl Pts',(-20.3460329085611,23.8953684980196,-69.539789838877));
#8205=CARTESIAN_POINT('Ctrl Pts',(-20.3453373457026,23.8888479442368,-69.5401926006131));
#8206=CARTESIAN_POINT('Ctrl Pts',(-20.3449962748506,23.8856038856906,-69.5403931033578));
#8207=CARTESIAN_POINT('Ctrl Pts',(-20.3441774102014,23.8776999633682,-69.5408819180821));
#8208=CARTESIAN_POINT('Ctrl Pts',(-20.3437048508246,23.873039574671,-69.5411703949735));
#8209=CARTESIAN_POINT('Ctrl Pts',(-20.3419568652735,23.8554182130945,-69.5422621361128));
#8210=CARTESIAN_POINT('Ctrl Pts',(-20.3407498616769,23.8424507168828,-69.5430675553196));
#8211=CARTESIAN_POINT('Ctrl Pts',(-20.3212162144471,23.6178448064226,-69.5570537791203));
#8212=CARTESIAN_POINT('Ctrl Pts',(-20.3237837381275,23.4049554090462,-69.5709144030612));
#8213=CARTESIAN_POINT('Ctrl Pts',(-20.3615357901215,23.0656276473282,-69.5938298851374));
#8214=CARTESIAN_POINT('Ctrl Pts',(-20.3834999463886,22.9383272821039,-69.6026042250923));
#8215=CARTESIAN_POINT('Ctrl Pts',(-20.4200818728375,22.7827261558073,-69.6133873773212));
#8216=CARTESIAN_POINT('Ctrl Pts',(-20.4275557080576,22.7528632352101,-69.6154592350294));
#8217=CARTESIAN_POINT('Ctrl Pts',(-20.4688210654069,22.5974687039588,-69.6262400979778));
#8218=CARTESIAN_POINT('Ctrl Pts',(-20.5097621395128,22.473942190946,-69.6348133008615));
#8219=CARTESIAN_POINT('Ctrl Pts',(-20.5610351204619,22.345777137666,-69.6434807911215));
#8220=CARTESIAN_POINT('Ctrl Pts',(-20.5640376800154,22.3383521359083,-69.643982078855));
#8221=CARTESIAN_POINT('Ctrl Pts',(-20.56817382582,22.3282326061923,-69.6446640490418));
#8222=CARTESIAN_POINT('Ctrl Pts',(-20.5692834116707,22.3255283946002,-69.6448461692418));
#8223=CARTESIAN_POINT('Ctrl Pts',(-20.5711460690098,22.3210063732845,-69.6451505066849));
#8224=CARTESIAN_POINT('Ctrl Pts',(-20.5718971260879,22.3191877438301,-69.6452728466501));
#8225=CARTESIAN_POINT('Ctrl Pts',(-20.5733795619881,22.3156074316168,-69.6455135838279));
#8226=CARTESIAN_POINT('Ctrl Pts',(-20.5741108393153,22.3138457103649,-69.6456319869689));
#8227=CARTESIAN_POINT('Ctrl Pts',(-20.5757266261717,22.3099628552812,-69.6458928330769));
#8228=CARTESIAN_POINT('Ctrl Pts',(-20.5766118429178,22.3078420125131,-69.6460352327587));
#8229=CARTESIAN_POINT('Ctrl Pts',(-20.5797119683309,22.3004368839684,-69.6465321745449));
#8230=CARTESIAN_POINT('Ctrl Pts',(-20.5819387169661,22.295157519204,-69.64688599722));
#8231=CARTESIAN_POINT('Ctrl Pts',(-20.6045926978961,22.241845045205,-69.6504545753356));
#8232=CARTESIAN_POINT('Ctrl Pts',(-20.6261713548739,22.1943056128722,-69.6536004119877));
#8233=CARTESIAN_POINT('Ctrl Pts',(-20.7741792290303,21.8882182996788,-69.6737491973082));
#8234=CARTESIAN_POINT('Ctrl Pts',(-20.9336143790115,21.647047594965,-69.6892248578868));
#8235=CARTESIAN_POINT('Ctrl Pts',(-21.2239227235977,21.3146646181717,-69.7142807460709));
#8236=CARTESIAN_POINT('Ctrl Pts',(-21.3329769434172,21.2064642814994,-69.7231852483819));
#8237=CARTESIAN_POINT('Ctrl Pts',(-21.4608049453515,21.0965703950268,-69.7333666947652));
#8238=CARTESIAN_POINT('Ctrl Pts',(-21.4723665163702,21.0867718763855,-69.7342853040387));
#8239=CARTESIAN_POINT('Ctrl Pts',(-21.4898488087919,21.072166130011,-69.7356711619499));
#8240=CARTESIAN_POINT('Ctrl Pts',(-21.4957182939447,21.0672976831511,-69.7361359165018));
#8241=CARTESIAN_POINT('Ctrl Pts',(-21.5052064443329,21.0594844113512,-69.7368863737828));
#8242=CARTESIAN_POINT('Ctrl Pts',(-21.508814345567,21.0565265121382,-69.7371715458267));
#8243=CARTESIAN_POINT('Ctrl Pts',(-21.5157298156449,21.0508820032858,-69.7377177916007));
#8244=CARTESIAN_POINT('Ctrl Pts',(-21.5190363173028,21.0481940970221,-69.7379788121445));
#8245=CARTESIAN_POINT('Ctrl Pts',(-21.5249188324979,21.043431455155,-69.7384429142217));
#8246=CARTESIAN_POINT('Ctrl Pts',(-21.5274927323596,21.0413541086916,-69.7386458900112));
#8247=CARTESIAN_POINT('Ctrl Pts',(-21.532583378152,21.037258469448,-69.7390471542757));
#8248=CARTESIAN_POINT('Ctrl Pts',(-21.5350999661484,21.0352399855055,-69.7392454347383));
#8249=CARTESIAN_POINT('Ctrl Pts',(-21.5411759148189,21.0303816135553,-69.7397239488418));
#8250=CARTESIAN_POINT('Ctrl Pts',(-21.5447382647403,21.0275454893941,-69.7400043331419));
#8251=CARTESIAN_POINT('Ctrl Pts',(-21.5578518052053,21.0171506254148,-69.7410358554184));
#8252=CARTESIAN_POINT('Ctrl Pts',(-21.5674397223444,21.0096385745877,-69.7417888559985));
#8253=CARTESIAN_POINT('Ctrl Pts',(-21.7240079052638,20.888394867784,-69.7540666413049));
#8254=CARTESIAN_POINT('Ctrl Pts',(-21.8804853066364,20.7875525532319,-69.7661049540718));
#8255=CARTESIAN_POINT('Ctrl Pts',(-22.1318220021524,20.654761274217,-69.7850621012348));
#8256=CARTESIAN_POINT('Ctrl Pts',(-22.2209506026328,20.6127757640286,-69.791711825621));
#8257=CARTESIAN_POINT('Ctrl Pts',(-22.5170429721264,20.4895352717375,-69.8134187578874));
#8258=CARTESIAN_POINT('Ctrl Pts',(-22.7305383827999,20.4255756397124,-69.8285154675558));
#8259=CARTESIAN_POINT('Ctrl Pts',(-22.9546402982399,20.3830144124232,-69.8428032229158));
#8260=CARTESIAN_POINT('Ctrl Pts',(-22.9603443162225,20.3819470641969,-69.8431658472457));
#8261=CARTESIAN_POINT('Ctrl Pts',(-22.9685750358209,20.3804299121675,-69.8436875744444));
#8262=CARTESIAN_POINT('Ctrl Pts',(-22.9710993982224,20.3799677185317,-69.8438473810731));
#8263=CARTESIAN_POINT('Ctrl Pts',(-22.9754916107563,20.3791689553197,-69.8441250698399));
#8264=CARTESIAN_POINT('Ctrl Pts',(-22.9773592083617,20.3788310200143,-69.8442430306244));
#8265=CARTESIAN_POINT('Ctrl Pts',(-22.9809753581909,20.3781799887585,-69.8444712106288));
#8266=CARTESIAN_POINT('Ctrl Pts',(-22.9827238663473,20.3778666894666,-69.8445814414945));
#8267=CARTESIAN_POINT('Ctrl Pts',(-22.9868985768621,20.3771222229283,-69.8448443891145));
#8268=CARTESIAN_POINT('Ctrl Pts',(-22.9893250208476,20.3766923916458,-69.8449970289975));
#8269=CARTESIAN_POINT('Ctrl Pts',(-22.9966627812733,20.3754012259567,-69.8454580511843));
#8270=CARTESIAN_POINT('Ctrl Pts',(-23.0015756353927,20.3745485011574,-69.8457659437666));
#8271=CARTESIAN_POINT('Ctrl Pts',(-23.0518132659927,20.36594880758,-69.8489066325906));
#8272=CARTESIAN_POINT('Ctrl Pts',(-23.0972997883876,20.3591608286777,-69.8516859010484));
#8273=CARTESIAN_POINT('Ctrl Pts',(-23.1453689344902,20.3530360961506,-69.8545700659835));
#8274=CARTESIAN_POINT('Ctrl Pts',(-23.1478194095478,20.3527267311312,-69.8547169508741));
#8275=CARTESIAN_POINT('Ctrl Pts',(-23.1570157531917,20.351576459898,-69.8552676587031));
#8276=CARTESIAN_POINT('Ctrl Pts',(-23.1637639669199,20.3507540761559,-69.8556706867813));
#8277=CARTESIAN_POINT('Ctrl Pts',(-23.1743133200474,20.3495023221859,-69.8562991195922));
#8278=CARTESIAN_POINT('Ctrl Pts',(-23.1781126709146,20.3490583609529,-69.856525123019));
#8279=CARTESIAN_POINT('Ctrl Pts',(-23.4706770996191,20.3153995523234,-69.8739037076153));
#8280=CARTESIAN_POINT('Ctrl Pts',(-23.7626367658595,20.3213919892458,-69.8895153890468));
#8281=CARTESIAN_POINT('Ctrl Pts',(-24.1929529271619,20.3889184871989,-69.9143151593598));
#8282=CARTESIAN_POINT('Ctrl Pts',(-24.3343497895245,20.4209906135522,-69.9227446799743));
#8283=CARTESIAN_POINT('Ctrl Pts',(-24.4871734345503,20.4666649213482,-69.9323822916213));
#8284=CARTESIAN_POINT('Ctrl Pts',(-24.5012181999091,20.4709672874008,-69.9332729086044));
#8285=CARTESIAN_POINT('Ctrl Pts',(-24.5223437132542,20.477597028551,-69.9346201314908));
#8286=CARTESIAN_POINT('Ctrl Pts',(-24.529446732089,20.4798532380009,-69.9350744073315));
#8287=CARTESIAN_POINT('Ctrl Pts',(-24.5409144501667,20.4835396951919,-69.9358099564711));
#8288=CARTESIAN_POINT('Ctrl Pts',(-24.5452840580032,20.4849546800023,-69.9360907273139));
#8289=CARTESIAN_POINT('Ctrl Pts',(-24.5536481498758,20.4876829444789,-69.9366291310175));
#8290=CARTESIAN_POINT('Ctrl Pts',(-24.5576431205322,20.4889947110628,-69.9368867135306));
#8291=CARTESIAN_POINT('Ctrl Pts',(-24.5647695065191,20.4913501525195,-69.9373469590184));
#8292=CARTESIAN_POINT('Ctrl Pts',(-24.5679019128772,20.4923908287431,-69.9375495225615));
#8293=CARTESIAN_POINT('Ctrl Pts',(-24.5741107365281,20.4944641768382,-69.9379515519471));
#8294=CARTESIAN_POINT('Ctrl Pts',(-24.5771872042629,20.4954966868786,-69.9381510122382));
#8295=CARTESIAN_POINT('Ctrl Pts',(-24.5855421248606,20.4983147749251,-69.938693392857));
#8296=CARTESIAN_POINT('Ctrl Pts',(-24.59081749663,20.5001093930799,-69.9390366126534));
#8297=CARTESIAN_POINT('Ctrl Pts',(-24.6105891054187,20.5068927203371,-69.9403258257028));
#8298=CARTESIAN_POINT('Ctrl Pts',(-24.6250541595463,20.5119711032113,-69.9412747943593));
#8299=CARTESIAN_POINT('Ctrl Pts',(-24.8594038779881,20.5961294444554,-69.9567446154558));
#8300=CARTESIAN_POINT('Ctrl Pts',(-25.0700366496534,20.6987731383425,-69.9720968042006));
#8301=CARTESIAN_POINT('Ctrl Pts',(-25.3408198647654,20.8693094536751,-69.9936665668001));
#8302=CARTESIAN_POINT('Ctrl Pts',(-25.4120689596462,20.9182900553482,-69.9995279332564));
#8303=CARTESIAN_POINT('Ctrl Pts',(-25.5553065080206,21.025489279465,-70.0116231064213));
#8304=CARTESIAN_POINT('Ctrl Pts',(-25.6269346998095,21.0840684946747,-70.0178489538812));
#8305=CARTESIAN_POINT('Ctrl Pts',(-25.7283111838244,21.1745295794955,-70.0268306845277));
#8306=CARTESIAN_POINT('Ctrl Pts',(-25.7600906410713,21.2040609553409,-70.0296724689211));
#8307=CARTESIAN_POINT('Ctrl Pts',(-25.8143888348437,21.2566004969746,-70.0345602380823));
#8308=CARTESIAN_POINT('Ctrl Pts',(-25.8371767164142,21.2793208266191,-70.0366219274718));
#8309=CARTESIAN_POINT('Ctrl Pts',(-25.8716445230647,21.3147315833281,-70.0397511298857));
#8310=CARTESIAN_POINT('Ctrl Pts',(-25.8835686177228,21.3271801616648,-70.0408357187708));
#8311=CARTESIAN_POINT('Ctrl Pts',(-25.8980347654528,21.3425272354005,-70.0421533706192));
#8312=CARTESIAN_POINT('Ctrl Pts',(-25.9006719509888,21.3453350831669,-70.0423936550143));
#8313=CARTESIAN_POINT('Ctrl Pts',(-25.9047893937255,21.34973476245,-70.0427689205692));
#8314=CARTESIAN_POINT('Ctrl Pts',(-25.9062730744668,21.3513233628658,-70.0429041661341));
#8315=CARTESIAN_POINT('Ctrl Pts',(-25.9088985025783,21.3541401578507,-70.0431435256301));
#8316=CARTESIAN_POINT('Ctrl Pts',(-25.9100408922806,21.355367735678,-70.0432476893965));
#8317=CARTESIAN_POINT('Ctrl Pts',(-25.912485791284,21.357999066242,-70.0434706436662));
#8318=CARTESIAN_POINT('Ctrl Pts',(-25.9137880040213,21.3594030844251,-70.0435894111368));
#8319=CARTESIAN_POINT('Ctrl Pts',(-25.9175640194288,21.3634815891704,-70.0439338513392));
#8320=CARTESIAN_POINT('Ctrl Pts',(-25.9200345496766,21.3661591219277,-70.0441592717809));
#8321=CARTESIAN_POINT('Ctrl Pts',(-25.9311381066062,21.3782340508269,-70.0451727213715));
#8322=CARTESIAN_POINT('Ctrl Pts',(-25.9397199678692,21.3876786517263,-70.0459568814096));
#8323=CARTESIAN_POINT('Ctrl Pts',(-25.9498109416931,21.3989174836971,-70.0468803286512));
#8324=CARTESIAN_POINT('Ctrl Pts',(-25.9513743154294,21.4006625169467,-70.0470234363668));
#8325=CARTESIAN_POINT('Ctrl Pts',(-26.1812518950587,21.6578148985226,-70.0680720734399));
#8326=CARTESIAN_POINT('Ctrl Pts',(-26.3674295842823,21.9480385579401,-70.0861980620253));
#8327=CARTESIAN_POINT('Ctrl Pts',(-26.5484479933871,22.3632042878768,-70.112021235616));
#8328=CARTESIAN_POINT('Ctrl Pts',(-26.5872755173855,22.4663948573075,-70.1184117394526));
#8329=CARTESIAN_POINT('Ctrl Pts',(-26.6357203618694,22.618352275501,-70.1279143731896));
#8330=CARTESIAN_POINT('Ctrl Pts',(-26.6496191056561,22.6656756548402,-70.1308856775448));
#8331=CARTESIAN_POINT('Ctrl Pts',(-26.6644782720238,22.7209286812893,-70.1343747157594));
#8332=CARTESIAN_POINT('Ctrl Pts',(-26.6665024547689,22.7285674181835,-70.134857508466));
#8333=CARTESIAN_POINT('Ctrl Pts',(-26.6695385679286,22.7401975082893,-70.1355932513166));
#8334=CARTESIAN_POINT('Ctrl Pts',(-26.6705709878878,22.7441835219459,-70.1358455364618));
#8335=CARTESIAN_POINT('Ctrl Pts',(-26.672348840822,22.7511021360537,-70.1362836488926));
#8336=CARTESIAN_POINT('Ctrl Pts',(-26.6730977896009,22.7540338347327,-70.1364693619936));
#8337=CARTESIAN_POINT('Ctrl Pts',(-26.6746462203631,22.760130832826,-70.1368557271043));
#8338=CARTESIAN_POINT('Ctrl Pts',(-26.6754450233196,22.7632962997588,-70.1370564008647));
#8339=CARTESIAN_POINT('Ctrl Pts',(-26.6776181846773,22.7719635151973,-70.1376060752315));
#8340=CARTESIAN_POINT('Ctrl Pts',(-26.6789828288816,22.7774676667662,-70.1379553896221));
#8341=CARTESIAN_POINT('Ctrl Pts',(-26.6841412823517,22.798511397466,-70.1392918469077));
#8342=CARTESIAN_POINT('Ctrl Pts',(-26.6878338551131,22.8140753393836,-70.1402822528392));
#8343=CARTESIAN_POINT('Ctrl Pts',(-26.7458671042957,23.0670519942177,-70.1564138368025));
#8344=CARTESIAN_POINT('Ctrl Pts',(-26.7732275270404,23.3097940514145,-70.1724632836176));
#8345=CARTESIAN_POINT('Ctrl Pts',(-26.7727713000577,23.8004142718755,-70.2055803345265));
#8346=CARTESIAN_POINT('Ctrl Pts',(-26.7441088293428,24.0467514073952,-70.2225345037189));
#8347=CARTESIAN_POINT('Ctrl Pts',(-26.6843247594727,24.3011915346032,-70.2390459835505));
#8348=CARTESIAN_POINT('Ctrl Pts',(-26.6809945986695,24.3149565546434,-70.2399358490089));
#8349=CARTESIAN_POINT('Ctrl Pts',(-26.6766691087743,24.3323337136085,-70.2410545399636));
#8350=CARTESIAN_POINT('Ctrl Pts',(-26.6757581410027,24.3359663950477,-70.2412881417185));
#8351=CARTESIAN_POINT('Ctrl Pts',(-26.6743087717276,24.3417036613345,-70.2416566604289));
#8352=CARTESIAN_POINT('Ctrl Pts',(-26.673774574792,24.3438092894938,-70.2417918207073));
#8353=CARTESIAN_POINT('Ctrl Pts',(-26.6727778470958,24.3477214619212,-70.2420427748023));
#8354=CARTESIAN_POINT('Ctrl Pts',(-26.6723158802198,24.3495281336152,-70.2421586003891));
#8355=CARTESIAN_POINT('Ctrl Pts',(-26.6712825230233,24.3535548475896,-70.2424166040518));
#8356=CARTESIAN_POINT('Ctrl Pts',(-26.6707103333404,24.3557746764691,-70.2425587346177));
#8357=CARTESIAN_POINT('Ctrl Pts',(-26.6690323276068,24.3622559366416,-70.2429734262373));
#8358=CARTESIAN_POINT('Ctrl Pts',(-26.667920141628,24.3665157365218,-70.2432456171354));
#8359=CARTESIAN_POINT('Ctrl Pts',(-26.6598317145208,24.3972376420547,-70.2452061285938));
#8360=CARTESIAN_POINT('Ctrl Pts',(-26.6525271229582,24.4236132545441,-70.2468756540591));
#8361=CARTESIAN_POINT('Ctrl Pts',(-26.6286584436974,24.5057180384982,-70.2520392229694));
#8362=CARTESIAN_POINT('Ctrl Pts',(-26.610921093037,24.56109680291,-70.2554734790134));
#8363=CARTESIAN_POINT('Ctrl Pts',(-26.5643876032176,24.693898455406,-70.263658288867));
#8364=CARTESIAN_POINT('Ctrl Pts',(-26.5340946061728,24.7707541349276,-70.2683527472317));
#8365=CARTESIAN_POINT('Ctrl Pts',(-26.3983109742341,25.0798685836107,-70.2873686658508));
#8366=CARTESIAN_POINT('Ctrl Pts',(-26.2683941139236,25.3003566998763,-70.3013326076835));
#8367=CARTESIAN_POINT('Ctrl Pts',(-26.0992935653018,25.5223286179826,-70.3176449710777));
#8368=CARTESIAN_POINT('Ctrl Pts',(-26.0845277947892,25.5412681345318,-70.3190558560882));
#8369=CARTESIAN_POINT('Ctrl Pts',(-26.0660276196305,25.5644583821631,-70.3208081727972));
#8370=CARTESIAN_POINT('Ctrl Pts',(-26.0624916474726,25.5688669390884,-70.321142415333));
#8371=CARTESIAN_POINT('Ctrl Pts',(-26.0564317940648,25.5763816206832,-70.3217140892147));
#8372=CARTESIAN_POINT('Ctrl Pts',(-26.0539136818858,25.5794923955847,-70.3219513084563));
#8373=CARTESIAN_POINT('Ctrl Pts',(-26.0478990935079,25.5868943397411,-70.3225171277646));
#8374=CARTESIAN_POINT('Ctrl Pts',(-26.0443973511884,25.5911811979813,-70.3228459227988));
#8375=CARTESIAN_POINT('Ctrl Pts',(-26.0365225776462,25.6007710187896,-70.3235839357552));
#8376=CARTESIAN_POINT('Ctrl Pts',(-26.0321435993699,25.6060690445317,-70.3239933768843));
#8377=CARTESIAN_POINT('Ctrl Pts',(-26.0248990257956,25.6147772063091,-70.3246692224832));
#8378=CARTESIAN_POINT('Ctrl Pts',(-26.022043236208,25.6181954989083,-70.3249352496621));
#8379=CARTESIAN_POINT('Ctrl Pts',(-26.0148305388406,25.6267925895438,-70.3256061717206));
#8380=CARTESIAN_POINT('Ctrl Pts',(-26.0104644017425,25.6319635871977,-70.3260114241569));
#8381=CARTESIAN_POINT('Ctrl Pts',(-26.0014342076304,25.6425903324593,-70.326847797595));
#8382=CARTESIAN_POINT('Ctrl Pts',(-25.9967681508325,25.6480443242752,-70.3272789961894));
#8383=CARTESIAN_POINT('Ctrl Pts',(-25.9730515156712,25.6755791261767,-70.3294658869556));
#8384=CARTESIAN_POINT('Ctrl Pts',(-25.9537205395439,25.6974156598916,-70.3312327891465));
#8385=CARTESIAN_POINT('Ctrl Pts',(-25.9297611094909,25.7237515523123,-70.3334052258832));
#8386=CARTESIAN_POINT('Ctrl Pts',(-25.9254116093061,25.728503761356,-70.3337989107911));
#8387=CARTESIAN_POINT('Ctrl Pts',(-25.9182171942355,25.7363171198167,-70.3344489769237));
#8388=CARTESIAN_POINT('Ctrl Pts',(-25.915380507959,25.7393858492691,-70.3347050066766));
#8389=CARTESIAN_POINT('Ctrl Pts',(-25.9102582607758,25.7449055229732,-70.3351668156039));
#8390=CARTESIAN_POINT('Ctrl Pts',(-25.9079748267202,25.7473584401178,-70.3353725034032));
#8391=CARTESIAN_POINT('Ctrl Pts',(-25.9030970596168,25.7525818886174,-70.3358115017229));
#8392=CARTESIAN_POINT('Ctrl Pts',(-25.9005016517379,25.7553514053228,-70.3360448583447));
#8393=CARTESIAN_POINT('Ctrl Pts',(-25.8935008303259,25.7627954651905,-70.3366736988925));
#8394=CARTESIAN_POINT('Ctrl Pts',(-25.8890863409604,25.7674614152416,-70.3370695746497));
#8395=CARTESIAN_POINT('Ctrl Pts',(-25.8675801120637,25.790056998115,-70.3389950651255));
#8396=CARTESIAN_POINT('Ctrl Pts',(-25.8502963619595,25.8078019743841,-70.340533019152));
#8397=CARTESIAN_POINT('Ctrl Pts',(-25.6182854776305,26.0405740879293,-70.3610584189883));
#8398=CARTESIAN_POINT('Ctrl Pts',(-25.3744413431208,26.2243337719409,-70.3815107714623));
#8399=CARTESIAN_POINT('Ctrl Pts',(-24.9814541353119,26.4414234148219,-70.4118758134113));
#8400=CARTESIAN_POINT('Ctrl Pts',(-24.8497243614881,26.5029780065853,-70.4216448297848));
#8401=CARTESIAN_POINT('Ctrl Pts',(-24.7131301523167,26.5558863625713,-70.4310984914138));
#8402=CARTESIAN_POINT('Ctrl Pts',(-24.7119789723293,26.5563314998846,-70.4311781167516));
#8403=CARTESIAN_POINT('Ctrl Pts',(-24.7079918478755,26.5578706054534,-70.4314537344056));
#8404=CARTESIAN_POINT('Ctrl Pts',(-24.705154602333,26.558961226336,-70.4316495745268));
#8405=CARTESIAN_POINT('Ctrl Pts',(-24.6660398962727,26.5739332134065,-70.4343454235395));
#8406=CARTESIAN_POINT('Ctrl Pts',(-24.6295138497505,26.5871624171628,-70.4368151094385));
#8407=CARTESIAN_POINT('Ctrl Pts',(-24.5878210460335,26.6014156436657,-70.4395732250138));
#8408=CARTESIAN_POINT('Ctrl Pts',(-24.5828823897317,26.6030906104339,-70.4398989711606));
#8409=CARTESIAN_POINT('Ctrl Pts',(-24.5756013273432,26.6055403244312,-70.4403777797364));
#8410=CARTESIAN_POINT('Ctrl Pts',(-24.5732620942583,26.6063243705401,-70.4405313911459));
#8411=CARTESIAN_POINT('Ctrl Pts',(-24.5691716417384,26.6076901540877,-70.4407996160293));
#8412=CARTESIAN_POINT('Ctrl Pts',(-24.5674208214995,26.6082730741243,-70.440914300176));
#8413=CARTESIAN_POINT('Ctrl Pts',(-24.5640742488086,26.6093840937031,-70.4411332748865));
#8414=CARTESIAN_POINT('Ctrl Pts',(-24.5624785888148,26.6099124469607,-70.4412375806105));
#8415=CARTESIAN_POINT('Ctrl Pts',(-24.5581812942722,26.6113316329999,-70.4415182141942));
#8416=CARTESIAN_POINT('Ctrl Pts',(-24.5554788843313,26.6122201401113,-70.4416944032691));
#8417=CARTESIAN_POINT('Ctrl Pts',(-24.5496696224129,26.6141216084974,-70.442072531881));
#8418=CARTESIAN_POINT('Ctrl Pts',(-24.5465623952858,26.6151334261082,-70.4422744039766));
#8419=CARTESIAN_POINT('Ctrl Pts',(-24.5378371260596,26.6179599960635,-70.4428402221975));
#8420=CARTESIAN_POINT('Ctrl Pts',(-24.5322155930431,26.619764050715,-70.443203548117));
#8421=CARTESIAN_POINT('Ctrl Pts',(-24.4812089082402,26.6359785815578,-70.4464893804643));
#8422=CARTESIAN_POINT('Ctrl Pts',(-24.4355116713999,26.6493978754957,-70.4493558598061));
#8423=CARTESIAN_POINT('Ctrl Pts',(-24.3321874209905,26.6772675478434,-70.4556993895046));
#8424=CARTESIAN_POINT('Ctrl Pts',(-24.2744239915123,26.6911475571649,-70.4591510517077));
#8425=CARTESIAN_POINT('Ctrl Pts',(-23.8387652513709,26.7831731355364,-70.4846989671614));
#8426=CARTESIAN_POINT('Ctrl Pts',(-23.4499915480244,26.7944776709091,-70.5052222929952));
#8427=CARTESIAN_POINT('Ctrl Pts',(-23.0486087575204,26.7337839447468,-70.5297769508713));
#8428=CARTESIAN_POINT('Ctrl Pts',(-23.0288333261363,26.7306048263253,-70.5309941847827));
#8429=CARTESIAN_POINT('Ctrl Pts',(-23.0029672781317,26.7261988439782,-70.5325965142103));
#8430=CARTESIAN_POINT('Ctrl Pts',(-22.9968484632859,26.7251383664122,-70.5329763070903));
#8431=CARTESIAN_POINT('Ctrl Pts',(-22.9874109180102,26.7234745942296,-70.5335632621162));
#8432=CARTESIAN_POINT('Ctrl Pts',(-22.9840899821133,26.7228837594877,-70.5337700268358));
#8433=CARTESIAN_POINT('Ctrl Pts',(-22.9774790468936,26.7216968835623,-70.5341820782333));
#8434=CARTESIAN_POINT('Ctrl Pts',(-22.9741890352289,26.7211009339034,-70.5343873617584));
#8435=CARTESIAN_POINT('Ctrl Pts',(-22.9668985420328,26.7197686195803,-70.534842752281));
#8436=CARTESIAN_POINT('Ctrl Pts',(-22.9628985200832,26.7190297995729,-70.5350929373806));
#8437=CARTESIAN_POINT('Ctrl Pts',(-22.9513633741587,26.7168766202313,-70.5358153699812));
#8438=CARTESIAN_POINT('Ctrl Pts',(-22.9438319228895,26.7154429500903,-70.5362882338329));
#8439=CARTESIAN_POINT('Ctrl Pts',(-22.8931372104116,26.7056052399919,-70.5394791386778));
#8440=CARTESIAN_POINT('Ctrl Pts',(-22.8501465250665,26.6963457486338,-70.5422244491292));
#8441=CARTESIAN_POINT('Ctrl Pts',(-22.7383682877288,26.6698660606305,-70.5494700621659));
#8442=CARTESIAN_POINT('Ctrl Pts',(-22.669939006162,26.6512509912246,-70.5540138063868));
#8443=CARTESIAN_POINT('Ctrl Pts',(-22.4599210496119,26.5866073808458,-70.568298840626));
#8444=CARTESIAN_POINT('Ctrl Pts',(-22.3208775763164,26.5330201220393,-70.5782540667229));
#8445=CARTESIAN_POINT('Ctrl Pts',(-22.1486907581259,26.4525692505281,-70.5910943196805));
#8446=CARTESIAN_POINT('Ctrl Pts',(-22.1116802286532,26.4344033675362,-70.5938850984888));
#8447=CARTESIAN_POINT('Ctrl Pts',(-22.0750359531635,26.415536742541,-70.5966750543042));
#8448=CARTESIAN_POINT('Ctrl Pts',(-22.0750360699906,26.4155368026905,-70.8406447795461));
#8449=CARTESIAN_POINT('Ctrl Pts',(-22.1568434848462,26.4576560598637,-70.8345484782489));
#8450=CARTESIAN_POINT('Ctrl Pts',(-22.2404443674471,26.496266412956,-70.828560865941));
#8451=CARTESIAN_POINT('Ctrl Pts',(-22.3331656296512,26.5343577118191,-70.8222657796152));
#8452=CARTESIAN_POINT('Ctrl Pts',(-22.3407313430195,26.5374322636108,-70.8217545830891));
#8453=CARTESIAN_POINT('Ctrl Pts',(-22.3510418599516,26.5415766538885,-70.8210613492461));
#8454=CARTESIAN_POINT('Ctrl Pts',(-22.3537764790467,26.5426715021678,-70.8208778121836));
#8455=CARTESIAN_POINT('Ctrl Pts',(-22.3583448235514,26.5444932482402,-70.8205717524333));
#8456=CARTESIAN_POINT('Ctrl Pts',(-22.360177715015,26.5452222116924,-70.8204491040594));
#8457=CARTESIAN_POINT('Ctrl Pts',(-22.3637811833146,26.5466515250489,-70.8202082687369));
#8458=CARTESIAN_POINT('Ctrl Pts',(-22.3655517111024,26.5473519884394,-70.8200900750433));
#8459=CARTESIAN_POINT('Ctrl Pts',(-22.3694480743911,26.5488894913646,-70.8198302706933));
#8460=CARTESIAN_POINT('Ctrl Pts',(-22.3715741852132,26.5497258417773,-70.8196887020245));
#8461=CARTESIAN_POINT('Ctrl Pts',(-22.3787590864162,26.552543354788,-70.8192109514106));
#8462=CARTESIAN_POINT('Ctrl Pts',(-22.383822032616,26.5545140001093,-70.8188754040773));
#8463=CARTESIAN_POINT('Ctrl Pts',(-22.4308167155575,26.5726689845069,-70.8157708640787));
#8464=CARTESIAN_POINT('Ctrl Pts',(-22.4730803274987,26.5879882518044,-70.8130528741506));
#8465=CARTESIAN_POINT('Ctrl Pts',(-22.5267828017507,26.6061918923568,-70.8096754184062));
#8466=CARTESIAN_POINT('Ctrl Pts',(-22.5379331442031,26.609903676736,-70.8089782486736));
#8467=CARTESIAN_POINT('Ctrl Pts',(-22.7993159653002,26.6953288540924,-70.7927257076985));
#8468=CARTESIAN_POINT('Ctrl Pts',(-23.0586315226244,26.7461488067811,-70.7784651185817));
#8469=CARTESIAN_POINT('Ctrl Pts',(-23.5065209382037,26.7780534544468,-70.7531071974504));
#8470=CARTESIAN_POINT('Ctrl Pts',(-23.692541691839,26.775209832435,-70.7423774027068));
#8471=CARTESIAN_POINT('Ctrl Pts',(-23.8863084304576,26.7554462237052,-70.7305466914208));
#8472=CARTESIAN_POINT('Ctrl Pts',(-23.8953463922374,26.7544857309435,-70.7299934316467));
#8473=CARTESIAN_POINT('Ctrl Pts',(-23.9116567044336,26.7526825750465,-70.7289923539003));
#8474=CARTESIAN_POINT('Ctrl Pts',(-23.9189305004199,26.7518533363886,-70.7285449610337));
#8475=CARTESIAN_POINT('Ctrl Pts',(-23.9301452383441,26.7505360914262,-70.7278536851682));
#8476=CARTESIAN_POINT('Ctrl Pts',(-23.9340882423245,26.7500655697134,-70.7276103551273));
#8477=CARTESIAN_POINT('Ctrl Pts',(-23.941349118929,26.7491855097309,-70.7271617470212));
#8478=CARTESIAN_POINT('Ctrl Pts',(-23.9446672472856,26.7487780936537,-70.7269565363545));
#8479=CARTESIAN_POINT('Ctrl Pts',(-23.9513416884471,26.7479480291313,-70.7265433437022));
#8480=CARTESIAN_POINT('Ctrl Pts',(-23.9546979814377,26.7475252576337,-70.726335358065));
#8481=CARTESIAN_POINT('Ctrl Pts',(-23.9642610271745,26.7463053609559,-70.7257421490837));
#8482=CARTESIAN_POINT('Ctrl Pts',(-23.9704661070976,26.7454954445138,-70.7253565211746));
#8483=CARTESIAN_POINT('Ctrl Pts',(-23.9969101901692,26.7419654754151,-70.7237100038563));
#8484=CARTESIAN_POINT('Ctrl Pts',(-24.0171251009287,26.7390712082845,-70.7224436060411));
#8485=CARTESIAN_POINT('Ctrl Pts',(-24.3755022789662,26.6842798673052,-70.6998512072786));
#8486=CARTESIAN_POINT('Ctrl Pts',(-24.7032382458937,26.5790584024982,-70.6766016889036));
#8487=CARTESIAN_POINT('Ctrl Pts',(-25.1458053302644,26.3545600222801,-70.6431762828056));
#8488=CARTESIAN_POINT('Ctrl Pts',(-25.2782516741849,26.2749473155368,-70.6329273010685));
#8489=CARTESIAN_POINT('Ctrl Pts',(-25.409191273214,26.182836290899,-70.6229005116117));
#8490=CARTESIAN_POINT('Ctrl Pts',(-25.4138760814877,26.1795219663123,-70.6225419279107));
#8491=CARTESIAN_POINT('Ctrl Pts',(-25.4206336580176,26.1747141014772,-70.6220249504299));
#8492=CARTESIAN_POINT('Ctrl Pts',(-25.4227135081198,26.1732306064876,-70.6218658705311));
#8493=CARTESIAN_POINT('Ctrl Pts',(-25.4263339287671,26.1706417678853,-70.621589023588));
#8494=CARTESIAN_POINT('Ctrl Pts',(-25.4278752895813,26.1695375365627,-70.6214711792857));
#8495=CARTESIAN_POINT('Ctrl Pts',(-25.430861527955,26.1673942040228,-70.6212429086787));
#8496=CARTESIAN_POINT('Ctrl Pts',(-25.4323065154895,26.1663552689686,-70.6211324712407));
#8497=CARTESIAN_POINT('Ctrl Pts',(-25.4357602564367,26.1638677130091,-70.6208685515591));
#8498=CARTESIAN_POINT('Ctrl Pts',(-25.4377682057396,26.1624179698686,-70.620715147479));
#8499=CARTESIAN_POINT('Ctrl Pts',(-25.4449638996919,26.1572100363396,-70.6201655243324));
#8500=CARTESIAN_POINT('Ctrl Pts',(-25.4501421521942,26.1534386623107,-70.6197702148695));
#8501=CARTESIAN_POINT('Ctrl Pts',(-25.5275203311578,26.0967294780353,-70.6138658294026));
#8502=CARTESIAN_POINT('Ctrl Pts',(-25.5975027934258,26.0408152382713,-70.6085606978806));
#8503=CARTESIAN_POINT('Ctrl Pts',(-25.8902445655522,25.7862317903975,-70.5860818100272));
#8504=CARTESIAN_POINT('Ctrl Pts',(-26.0871374555623,25.5600806093899,-70.5700667804063));
#8505=CARTESIAN_POINT('Ctrl Pts',(-26.2948877096018,25.241352581633,-70.5481095922781));
#8506=CARTESIAN_POINT('Ctrl Pts',(-26.337023228474,25.1709774098234,-70.5433049373713));
#8507=CARTESIAN_POINT('Ctrl Pts',(-26.3970718102084,25.0614053487511,-70.5358369958345));
#8508=CARTESIAN_POINT('Ctrl Pts',(-26.4169603498093,25.0233271581647,-70.5332442313067));
#8509=CARTESIAN_POINT('Ctrl Pts',(-26.4394724278771,24.9780424289846,-70.5301596689538));
#8510=CARTESIAN_POINT('Ctrl Pts',(-26.4428394527522,24.9712087244939,-70.529694165817));
#8511=CARTESIAN_POINT('Ctrl Pts',(-26.4479625776008,24.96071717696,-70.5289794311797));
#8512=CARTESIAN_POINT('Ctrl Pts',(-26.4497360684655,24.9570678164584,-70.5287308074063));
#8513=CARTESIAN_POINT('Ctrl Pts',(-26.4529582921737,24.9504053833599,-70.5282768833974));
#8514=CARTESIAN_POINT('Ctrl Pts',(-26.454409239218,24.9473933828464,-70.5280716606924));
#8515=CARTESIAN_POINT('Ctrl Pts',(-26.4573175139039,24.9413320312493,-70.5276586489568));
#8516=CARTESIAN_POINT('Ctrl Pts',(-26.4587747367852,24.9382826348356,-70.5274508566037));
#8517=CARTESIAN_POINT('Ctrl Pts',(-26.4629097602464,24.9295945476515,-70.5268587975263));
#8518=CARTESIAN_POINT('Ctrl Pts',(-26.4655759678214,24.9239503841758,-70.5264741287578));
#8519=CARTESIAN_POINT('Ctrl Pts',(-26.4768397958023,24.8999252065921,-70.5248365270691));
#8520=CARTESIAN_POINT('Ctrl Pts',(-26.4852799560693,24.8814712709094,-70.5235781591521));
#8521=CARTESIAN_POINT('Ctrl Pts',(-26.6424991168747,24.5289560777802,-70.4995265927446));
#8522=CARTESIAN_POINT('Ctrl Pts',(-26.7334890350843,24.1721084327779,-70.4744903825534));
#8523=CARTESIAN_POINT('Ctrl Pts',(-26.7695858619726,23.7218455905839,-70.4442180147743));
#8524=CARTESIAN_POINT('Ctrl Pts',(-26.7730246589785,23.6356536313015,-70.4385046968183));
#8525=CARTESIAN_POINT('Ctrl Pts',(-26.7729907852082,23.5042804733903,-70.4300140636944));
#8526=CARTESIAN_POINT('Ctrl Pts',(-26.7720307068816,23.4591416663388,-70.4271360544965));
#8527=CARTESIAN_POINT('Ctrl Pts',(-26.7698925606029,23.4086007306609,-70.4239686538314));
#8528=CARTESIAN_POINT('Ctrl Pts',(-26.7696488954935,23.4031668346537,-70.4236288257262));
#8529=CARTESIAN_POINT('Ctrl Pts',(-26.7692832932904,23.3954502596045,-70.4231472815852));
#8530=CARTESIAN_POINT('Ctrl Pts',(-26.7691726848207,23.3931670918134,-70.4230049323471));
#8531=CARTESIAN_POINT('Ctrl Pts',(-26.7689654751555,23.3889820241303,-70.4227442442523));
#8532=CARTESIAN_POINT('Ctrl Pts',(-26.7688696172047,23.3870800893672,-70.4226258632761));
#8533=CARTESIAN_POINT('Ctrl Pts',(-26.7686710585271,23.3832087115309,-70.4223850854739));
#8534=CARTESIAN_POINT('Ctrl Pts',(-26.7685682358629,23.3812392775772,-70.4222626957298));
#8535=CARTESIAN_POINT('Ctrl Pts',(-26.7683074276147,23.3763303804245,-70.4219578754441));
#8536=CARTESIAN_POINT('Ctrl Pts',(-26.7681472218615,23.3733910293306,-70.4217755707522));
#8537=CARTESIAN_POINT('Ctrl Pts',(-26.7675281322249,23.3623117387532,-70.4210892093462));
#8538=CARTESIAN_POINT('Ctrl Pts',(-26.7670423828434,23.3541732406579,-70.4205866564937));
#8539=CARTESIAN_POINT('Ctrl Pts',(-26.7576558439059,23.2063411444308,-70.4114861566057));
#8540=CARTESIAN_POINT('Ctrl Pts',(-26.7396926774909,23.0673511729968,-70.4033843704302));
#8541=CARTESIAN_POINT('Ctrl Pts',(-26.6447873028743,22.5834926157689,-70.3754362690836));
#8542=CARTESIAN_POINT('Ctrl Pts',(-26.5203772922803,22.2505870940093,-70.3563715356991));
#8543=CARTESIAN_POINT('Ctrl Pts',(-26.3342669732415,21.9267379737192,-70.3337839927446));
#8544=CARTESIAN_POINT('Ctrl Pts',(-26.3239070427488,21.9091015471656,-70.3325411310172));
#8545=CARTESIAN_POINT('Ctrl Pts',(-26.310157332583,21.8861965646208,-70.3309097856292));
#8546=CARTESIAN_POINT('Ctrl Pts',(-26.3069189289913,21.8808373213106,-70.3305268470205));
#8547=CARTESIAN_POINT('Ctrl Pts',(-26.3019065784676,21.8725967212578,-70.3299360965051));
#8548=CARTESIAN_POINT('Ctrl Pts',(-26.3001436655819,21.8697086426385,-70.3297286903959));
#8549=CARTESIAN_POINT('Ctrl Pts',(-26.2966299688226,21.8639726880741,-70.3293160343098));
#8550=CARTESIAN_POINT('Ctrl Pts',(-26.294879295434,21.86112474914,-70.3291107885816));
#8551=CARTESIAN_POINT('Ctrl Pts',(-26.2909972798832,21.8548315810051,-70.3286564534698));
#8552=CARTESIAN_POINT('Ctrl Pts',(-26.2888638687847,21.8513876403974,-70.3284072878832));
#8553=CARTESIAN_POINT('Ctrl Pts',(-26.2827154698159,21.8415040294614,-70.3276906872481));
#8554=CARTESIAN_POINT('Ctrl Pts',(-26.2786842425549,21.835074538108,-70.3272226512513));
#8555=CARTESIAN_POINT('Ctrl Pts',(-26.2520026432515,21.7928515784222,-70.3241365891549));
#8556=CARTESIAN_POINT('Ctrl Pts',(-26.2286720828989,21.7574948215304,-70.3214933022386));
#8557=CARTESIAN_POINT('Ctrl Pts',(-26.1578474666666,21.6546318228771,-70.3136222322753));
#8558=CARTESIAN_POINT('Ctrl Pts',(-26.1084523159659,21.5884826354331,-70.3083233744047));
#8559=CARTESIAN_POINT('Ctrl Pts',(-25.8691902383273,21.292488459127,-70.2834878438769));
#8560=CARTESIAN_POINT('Ctrl Pts',(-25.6505876051953,21.0878308124263,-70.2628606417758));
#8561=CARTESIAN_POINT('Ctrl Pts',(-25.3334292928987,20.8642700355719,-70.2371946342417));
#8562=CARTESIAN_POINT('Ctrl Pts',(-25.2577013936905,20.8155051494572,-70.2313498034771));
#8563=CARTESIAN_POINT('Ctrl Pts',(-25.1744897620466,20.7667274071141,-70.2253030747068));
#8564=CARTESIAN_POINT('Ctrl Pts',(-25.1689467996445,20.7635003776245,-70.2249020238984));
#8565=CARTESIAN_POINT('Ctrl Pts',(-25.1612490436761,20.7590495758212,-70.2243475135749));
#8566=CARTESIAN_POINT('Ctrl Pts',(-25.1591024648436,20.7578117364044,-70.2241931470206));
#8567=CARTESIAN_POINT('Ctrl Pts',(-25.1554113936087,20.7556889237034,-70.223928166054));
#8568=CARTESIAN_POINT('Ctrl Pts',(-25.1538675960381,20.7548027545503,-70.223817473633));
#8569=CARTESIAN_POINT('Ctrl Pts',(-25.1506780338116,20.752975396867,-70.223589060378));
#8570=CARTESIAN_POINT('Ctrl Pts',(-25.1490321759769,20.7520343833191,-70.2234713514695));
#8571=CARTESIAN_POINT('Ctrl Pts',(-25.145167640129,20.7498293708869,-70.2231953292544));
#8572=CARTESIAN_POINT('Ctrl Pts',(-25.1429482826786,20.7485665522161,-70.2230370930785));
#8573=CARTESIAN_POINT('Ctrl Pts',(-25.1360771244657,20.7446676530103,-70.2225480506317));
#8574=CARTESIAN_POINT('Ctrl Pts',(-25.1314202323325,20.7420404930526,-70.222217820715));
#8575=CARTESIAN_POINT('Ctrl Pts',(-25.1204323587239,20.7358777424988,-70.2214414572104));
#8576=CARTESIAN_POINT('Ctrl Pts',(-25.1140959091309,20.7323518882253,-70.2209959365115));
#8577=CARTESIAN_POINT('Ctrl Pts',(-25.0483780790752,20.6960737969633,-70.2163973247492));
#8578=CARTESIAN_POINT('Ctrl Pts',(-24.9879838837496,20.6651794812264,-70.2123571893629));
#8579=CARTESIAN_POINT('Ctrl Pts',(-24.8869146166182,20.6174409696595,-70.2058239457316));
#8580=CARTESIAN_POINT('Ctrl Pts',(-24.846793087314,20.5994844867096,-70.2032876258301));
#8581=CARTESIAN_POINT('Ctrl Pts',(-24.5380927814879,20.4688375136681,-70.1841152455068));
#8582=CARTESIAN_POINT('Ctrl Pts',(-24.2557246272593,20.3922041578629,-70.1683990101405));
#8583=CARTESIAN_POINT('Ctrl Pts',(-23.8679499868752,20.3416482215355,-70.1456452288007));
#8584=CARTESIAN_POINT('Ctrl Pts',(-23.7684722534536,20.3333517972032,-70.1397229675672));
#8585=CARTESIAN_POINT('Ctrl Pts',(-23.6594109589498,20.3293380900479,-70.1330802995748));
#8586=CARTESIAN_POINT('Ctrl Pts',(-23.6500436117652,20.3290342621462,-70.132508572211));
#8587=CARTESIAN_POINT('Ctrl Pts',(-23.6361456577979,20.328644165389,-70.1316585232879));
#8588=CARTESIAN_POINT('Ctrl Pts',(-23.6316159213539,20.3285265822315,-70.1313811847045));
#8589=CARTESIAN_POINT('Ctrl Pts',(-23.6238667159252,20.3283417812433,-70.130906239806));
#8590=CARTESIAN_POINT('Ctrl Pts',(-23.6206473571777,20.3282698345924,-70.130708782147));
#8591=CARTESIAN_POINT('Ctrl Pts',(-23.6143885523189,20.3281393469914,-70.1303246181164));
#8592=CARTESIAN_POINT('Ctrl Pts',(-23.6113491201028,20.3280802813381,-70.1301379284605));
#8593=CARTESIAN_POINT('Ctrl Pts',(-23.60408642782,20.3279494244053,-70.1296915227256));
#8594=CARTESIAN_POINT('Ctrl Pts',(-23.5998631094838,20.3278816353021,-70.1294316812858));
#8595=CARTESIAN_POINT('Ctrl Pts',(-23.5873940382827,20.3277060114427,-70.1286637638229));
#8596=CARTESIAN_POINT('Ctrl Pts',(-23.5791480371971,20.3276215235842,-70.1281549556894));
#8597=CARTESIAN_POINT('Ctrl Pts',(-23.5167913918398,20.3272219736655,-70.1242998572468));
#8598=CARTESIAN_POINT('Ctrl Pts',(-23.4626836377807,20.3282381401279,-70.1209119896705));
#8599=CARTESIAN_POINT('Ctrl Pts',(-23.2790364336706,20.3363162714833,-70.1092581570401));
#8600=CARTESIAN_POINT('Ctrl Pts',(-23.1499211179655,20.3498350401953,-70.1007959728171));
#8601=CARTESIAN_POINT('Ctrl Pts',(-22.7907392180615,20.4095188907948,-70.0765658497809));
#8602=CARTESIAN_POINT('Ctrl Pts',(-22.5643929998235,20.4730555631309,-70.0604409076954));
#8603=CARTESIAN_POINT('Ctrl Pts',(-22.2604450512975,20.5953906309131,-70.0387407774199));
#8604=CARTESIAN_POINT('Ctrl Pts',(-22.1754852917749,20.6339481752089,-70.0326790631893));
#8605=CARTESIAN_POINT('Ctrl Pts',(-22.0865438772052,20.6790652638132,-70.0264266033907));
#8606=CARTESIAN_POINT('Ctrl Pts',(-22.0807874485577,20.6820071231527,-70.0260223670662));
#8607=CARTESIAN_POINT('Ctrl Pts',(-22.0728293885409,20.6861043860963,-70.0254641655527));
#8608=CARTESIAN_POINT('Ctrl Pts',(-22.0706202338591,20.6872450208479,-70.025309277587));
#8609=CARTESIAN_POINT('Ctrl Pts',(-22.0668296962131,20.6892077172628,-70.0250436366114));
#8610=CARTESIAN_POINT('Ctrl Pts',(-22.0652476756486,20.690028534073,-70.0249328047202));
#8611=CARTESIAN_POINT('Ctrl Pts',(-22.0621536215228,20.6916371146009,-70.0247161160105));
#8612=CARTESIAN_POINT('Ctrl Pts',(-22.0606415358581,20.6924247638974,-70.0246102525814));
#8613=CARTESIAN_POINT('Ctrl Pts',(-22.0569719596457,20.6943399591972,-70.0243534207472));
#8614=CARTESIAN_POINT('Ctrl Pts',(-22.0548151150017,20.6954687532875,-70.0242025320468));
#8615=CARTESIAN_POINT('Ctrl Pts',(-22.048232751481,20.6989231687534,-70.0237422433672));
#8616=CARTESIAN_POINT('Ctrl Pts',(-22.0438113365543,20.7012566590219,-70.0234333420699));
#8617=CARTESIAN_POINT('Ctrl Pts',(-21.9997705414853,20.7246312584567,-70.0203590318891));
#8618=CARTESIAN_POINT('Ctrl Pts',(-21.9605867014153,20.7464884490534,-70.0176447073522));
#8619=CARTESIAN_POINT('Ctrl Pts',(-21.8501714376273,20.8111386528365,-70.0100194533269));
#8620=CARTESIAN_POINT('Ctrl Pts',(-21.780117864996,20.855879520925,-70.0052096887058));
#8621=CARTESIAN_POINT('Ctrl Pts',(-21.5234094871498,21.0341696885261,-69.9873918105921));
#8622=CARTESIAN_POINT('Ctrl Pts',(-21.3494672165008,21.18481040924,-69.9748711948285));
#8623=CARTESIAN_POINT('Ctrl Pts',(-21.0895719395568,21.4635874314477,-69.9531234034569));
#8624=CARTESIAN_POINT('Ctrl Pts',(-20.9941239734929,21.5816699427553,-69.944258149534));
#8625=CARTESIAN_POINT('Ctrl Pts',(-20.9009332523282,21.7152182888218,-69.9343531599254));
#8626=CARTESIAN_POINT('Ctrl Pts',(-20.8945641016132,21.7244479764672,-69.93366927389));
#8627=CARTESIAN_POINT('Ctrl Pts',(-20.8857655242585,21.7373416476576,-69.9327147443955));
#8628=CARTESIAN_POINT('Ctrl Pts',(-20.8832951755805,21.7409777193421,-69.9324456558294));
#8629=CARTESIAN_POINT('Ctrl Pts',(-20.879048351611,21.7472561565554,-69.9319811733108));
#8630=CARTESIAN_POINT('Ctrl Pts',(-20.8772683338622,21.7498961285093,-69.9317859137423));
#8631=CARTESIAN_POINT('Ctrl Pts',(-20.8735981520945,21.7553568733975,-69.9313821171932));
#8632=CARTESIAN_POINT('Ctrl Pts',(-20.8717085288561,21.7581780029079,-69.9311735601583));
#8633=CARTESIAN_POINT('Ctrl Pts',(-20.8673130978452,21.7647626828779,-69.9306868948891));
#8634=CARTESIAN_POINT('Ctrl Pts',(-20.8648107494876,21.7685285238932,-69.9304086567612));
#8635=CARTESIAN_POINT('Ctrl Pts',(-20.8569889518525,21.7803536361193,-69.9295352358262));
#8636=CARTESIAN_POINT('Ctrl Pts',(-20.8516978325178,21.7884315012388,-69.9289389904849));
#8637=CARTESIAN_POINT('Ctrl Pts',(-20.8008600368129,21.8668110272988,-69.9231572201251));
#8638=CARTESIAN_POINT('Ctrl Pts',(-20.7580380981302,21.9388336449791,-69.9178709842721));
#8639=CARTESIAN_POINT('Ctrl Pts',(-20.6848790194872,22.0735700180661,-69.9080153995873));
#8640=CARTESIAN_POINT('Ctrl Pts',(-20.6536752100424,22.1357577983018,-69.9034792300966));
#8641=CARTESIAN_POINT('Ctrl Pts',(-20.5400404612068,22.3817830441713,-69.8855972627026));
#8642=CARTESIAN_POINT('Ctrl Pts',(-20.4729092667373,22.5721706731769,-69.8718592193798));
#8643=CARTESIAN_POINT('Ctrl Pts',(-20.3874640202931,22.9134573920773,-69.8481565870541));
#8644=CARTESIAN_POINT('Ctrl Pts',(-20.3611892283964,23.0617582858008,-69.8381578137268));
#8645=CARTESIAN_POINT('Ctrl Pts',(-20.3443779686358,23.2207457145788,-69.8281030122695));
#8646=CARTESIAN_POINT('Ctrl Pts',(-20.3434276800245,23.2301262556892,-69.827512224363));
#8647=CARTESIAN_POINT('Ctrl Pts',(-20.3422068941983,23.2427282267751,-69.8267219794453));
#8648=CARTESIAN_POINT('Ctrl Pts',(-20.3419000689391,23.2459459669852,-69.8265205012553));
#8649=CARTESIAN_POINT('Ctrl Pts',(-20.3414269049889,23.2509884058773,-69.8262052456934));
#8650=CARTESIAN_POINT('Ctrl Pts',(-20.3412572815605,23.2528127827339,-69.8260912823823));
#8651=CARTESIAN_POINT('Ctrl Pts',(-20.3409344753468,23.2563171281779,-69.8258725651676));
#8652=CARTESIAN_POINT('Ctrl Pts',(-20.34078105677,23.257997061427,-69.8257677986879));
#8653=CARTESIAN_POINT('Ctrl Pts',(-20.340420840475,23.2619759209309,-69.82551985991));
#8654=CARTESIAN_POINT('Ctrl Pts',(-20.3402151936876,23.2642749469916,-69.825376753665));
#8655=CARTESIAN_POINT('Ctrl Pts',(-20.3396257815547,23.2709450183455,-69.8249620107601));
#8656=CARTESIAN_POINT('Ctrl Pts',(-20.3392484710037,23.2753166509965,-69.824690738884));
#8657=CARTESIAN_POINT('Ctrl Pts',(-20.3365877649467,23.3068971094282,-69.8227350031928));
#8658=CARTESIAN_POINT('Ctrl Pts',(-20.3346412192299,23.3341342740311,-69.8210692477161));
#8659=CARTESIAN_POINT('Ctrl Pts',(-20.3296538775864,23.4190937949285,-69.8159296134922));
#8660=CARTESIAN_POINT('Ctrl Pts',(-20.3278193857779,23.476878147688,-69.8125147198375));
#8661=CARTESIAN_POINT('Ctrl Pts',(-20.3264883972116,23.7523985662997,-69.7964858632678));
#8662=CARTESIAN_POINT('Ctrl Pts',(-20.3475008460763,23.9696751011115,-69.7845670812664));
#8663=CARTESIAN_POINT('Ctrl Pts',(-20.4305871968124,24.3844918948921,-69.7607722444885));
#8664=CARTESIAN_POINT('Ctrl Pts',(-20.4900437167122,24.5814508194212,-69.7489813346355));
#8665=CARTESIAN_POINT('Ctrl Pts',(-20.5725955817651,24.783068651061,-69.7357426286716));
#8666=CARTESIAN_POINT('Ctrl Pts',(-20.5774408797817,24.7947071796445,-69.7349742724588));
#8667=CARTESIAN_POINT('Ctrl Pts',(-20.5841552373398,24.810572235037,-69.7339211136233));
#8668=CARTESIAN_POINT('Ctrl Pts',(-20.5859653296447,24.814823722895,-69.7336383210512));
#8669=CARTESIAN_POINT('Ctrl Pts',(-20.5890619582041,24.822053804361,-69.7331564287968));
#8670=CARTESIAN_POINT('Ctrl Pts',(-20.5903438644285,24.8250343840177,-69.7329574874337));
#8671=CARTESIAN_POINT('Ctrl Pts',(-20.5928322858199,24.8307962611718,-69.7325723565989));
#8672=CARTESIAN_POINT('Ctrl Pts',(-20.5940382291064,24.833577802578,-69.7323861868843));
#8673=CARTESIAN_POINT('Ctrl Pts',(-20.596909589863,24.8401751512617,-69.7319440323076));
#8674=CARTESIAN_POINT('Ctrl Pts',(-20.5985784772506,24.8439894340826,-69.7316879287443));
#8675=CARTESIAN_POINT('Ctrl Pts',(-20.603438172643,24.8550380361116,-69.7309447185005));
#8676=CARTESIAN_POINT('Ctrl Pts',(-20.6066482016818,24.8622638219634,-69.7304569524115));
#8677=CARTESIAN_POINT('Ctrl Pts',(-20.6305953771663,24.9156387166601,-69.7268412073946));
#8678=CARTESIAN_POINT('Ctrl Pts',(-20.6523891177638,24.9613033804865,-69.7236769203354));
#8679=CARTESIAN_POINT('Ctrl Pts',(-20.7273626230876,25.1093269424432,-69.7131768208526));
#8680=CARTESIAN_POINT('Ctrl Pts',(-20.7849578018111,25.2093367382236,-69.7056892046097));
#8681=CARTESIAN_POINT('Ctrl Pts',(-20.9333841637604,25.4377918353639,-69.6876564650926));
#8682=CARTESIAN_POINT('Ctrl Pts',(-21.0285013279266,25.5631036187459,-69.6770040138043));
#8683=CARTESIAN_POINT('Ctrl Pts',(-21.2531133407459,25.8179875226884,-69.6540230220447));
#8684=CARTESIAN_POINT('Ctrl Pts',(-21.3853024261898,25.9445120998659,-69.6417424715827));
#8685=CARTESIAN_POINT('Ctrl Pts',(-21.5362479854762,26.0662074351165,-69.6295268339463));
#8686=CARTESIAN_POINT('Ctrl Pts',(-21.5450174463286,26.0732023230106,-69.6288231773924));
#8687=CARTESIAN_POINT('Ctrl Pts',(-21.5565434756871,26.0822979042653,-69.627906401276));
#8688=CARTESIAN_POINT('Ctrl Pts',(-21.5592670234869,26.0844400297183,-69.62769035684));
#8689=CARTESIAN_POINT('Ctrl Pts',(-21.5634729299505,26.0877370947517,-69.6273576338531));
#8690=CARTESIAN_POINT('Ctrl Pts',(-21.5649528420535,26.0888951288345,-69.6272407333328));
#8691=CARTESIAN_POINT('Ctrl Pts',(-21.5677570994235,26.0910855138363,-69.6270195497289));
#8692=CARTESIAN_POINT('Ctrl Pts',(-21.5690812319002,26.09211811882,-69.6269152486059));
#8693=CARTESIAN_POINT('Ctrl Pts',(-21.5721611450506,26.0945160745441,-69.6266729677339));
#8694=CARTESIAN_POINT('Ctrl Pts',(-21.5739175296328,26.0958806406464,-69.6265350446998));
#8695=CARTESIAN_POINT('Ctrl Pts',(-21.5775362330363,26.0986860724774,-69.6262513758983));
#8696=CARTESIAN_POINT('Ctrl Pts',(-21.5793987218562,26.10012671822,-69.6261056458687));
#8697=CARTESIAN_POINT('Ctrl Pts',(-21.588839034558,26.107412331672,-69.6253683462196));
#8698=CARTESIAN_POINT('Ctrl Pts',(-21.5964413942384,26.1132256478236,-69.624779010673));
#8699=CARTESIAN_POINT('Ctrl Pts',(-21.6158851787148,26.1279569851182,-69.6232826277794));
#8700=CARTESIAN_POINT('Ctrl Pts',(-21.6277625868296,26.136827436156,-69.6223787744855));
#8701=CARTESIAN_POINT('Ctrl Pts',(-21.6769670915504,26.1730488549657,-69.6186743800444));
#8702=CARTESIAN_POINT('Ctrl Pts',(-21.7148218037523,26.1996776426251,-69.6159185185576));
#8703=CARTESIAN_POINT('Ctrl Pts',(-21.804750299189,26.2600846643298,-69.6095552841573));
#8704=CARTESIAN_POINT('Ctrl Pts',(-21.8572529567166,26.2931928257681,-69.6059791495121));
#8705=CARTESIAN_POINT('Ctrl Pts',(-21.9645883187378,26.3566215932559,-69.5988755996711));
#8706=CARTESIAN_POINT('Ctrl Pts',(-22.0193969537009,26.3868905215353,-69.5953515269656));
#8707=CARTESIAN_POINT('Ctrl Pts',(-22.0750360905742,26.4155368132881,-69.5918437005959));
#8708=CARTESIAN_POINT('Origin',(-23.5502525316942,23.5502525316942,-77.3107734492734));
#8709=CARTESIAN_POINT('',(-22.0750358851076,26.4155367075019,-68.0965974740783));
#8710=CARTESIAN_POINT('',(-22.0750360157945,26.4155367747871,-68.3458849806668));
#8711=CARTESIAN_POINT('',(-22.0750360153461,26.4155367745563,-77.3107734492734));
#8712=CARTESIAN_POINT('',(-26.7730025010771,23.5498082993017,-68.9362096369654));
#8713=CARTESIAN_POINT('Ctrl Pts',(-22.0750358851076,26.4155367075019,-68.0965974740783));
#8714=CARTESIAN_POINT('Ctrl Pts',(-21.9058636254286,26.3284368883194,-68.1072292468121));
#8715=CARTESIAN_POINT('Ctrl Pts',(-21.7446756452602,26.2264947685448,-68.1178689864256));
#8716=CARTESIAN_POINT('Ctrl Pts',(-21.5250098919503,26.0586210667221,-68.1340512927263));
#8717=CARTESIAN_POINT('Ctrl Pts',(-21.4587723498944,26.0036642502873,-68.1391782460546));
#8718=CARTESIAN_POINT('Ctrl Pts',(-21.3873648520484,25.9394228739606,-68.1450261979675));
#8719=CARTESIAN_POINT('Ctrl Pts',(-21.379944287117,25.9326840961005,-68.1456379302412));
#8720=CARTESIAN_POINT('Ctrl Pts',(-21.3692469938658,25.9228781972286,-68.1465256858236));
#8721=CARTESIAN_POINT('Ctrl Pts',(-21.3659449931704,25.919838630914,-68.1468005351226));
#8722=CARTESIAN_POINT('Ctrl Pts',(-21.3602017462695,25.9145296368036,-68.1472800242483));
#8723=CARTESIAN_POINT('Ctrl Pts',(-21.3577576457835,25.912263295346,-68.1474845318119));
#8724=CARTESIAN_POINT('Ctrl Pts',(-21.3527443059223,25.9076000890446,-68.1479049578816));
#8725=CARTESIAN_POINT('Ctrl Pts',(-21.3501754625055,25.9052028067436,-68.1481208941756));
#8726=CARTESIAN_POINT('Ctrl Pts',(-21.3449707947261,25.9003297857386,-68.1485594349083));
#8727=CARTESIAN_POINT('Ctrl Pts',(-21.3423352070932,25.8978538025531,-68.1487820497302));
#8728=CARTESIAN_POINT('Ctrl Pts',(-21.3359776767361,25.8918610919549,-68.1493203545271));
#8729=CARTESIAN_POINT('Ctrl Pts',(-21.3322599461595,25.8883399280107,-68.1496362362988));
#8730=CARTESIAN_POINT('Ctrl Pts',(-21.3222314156805,25.8787961896121,-68.1504912982551));
#8731=CARTESIAN_POINT('Ctrl Pts',(-21.3159366848155,25.8727568598306,-68.1510312064061));
#8732=CARTESIAN_POINT('Ctrl Pts',(-21.1977632492247,25.7584531061814,-68.1612280009303));
#8733=CARTESIAN_POINT('Ctrl Pts',(-21.0938677304,25.6422650103483,-68.1712414689084));
#8734=CARTESIAN_POINT('Ctrl Pts',(-20.8357977984593,25.3078171295318,-68.1991767975091));
#8735=CARTESIAN_POINT('Ctrl Pts',(-20.6996870655115,25.0771961115418,-68.2176063925051));
#8736=CARTESIAN_POINT('Ctrl Pts',(-20.586043536998,24.8151394130983,-68.2364398246966));
#8737=CARTESIAN_POINT('Ctrl Pts',(-20.5786864800503,24.7977576478982,-68.2376791711917));
#8738=CARTESIAN_POINT('Ctrl Pts',(-20.5687076949423,24.773592549043,-68.23938767852));
#8739=CARTESIAN_POINT('Ctrl Pts',(-20.5659557016669,24.7668637447017,-68.2398618670843));
#8740=CARTESIAN_POINT('Ctrl Pts',(-20.5628863940264,24.7592860062701,-68.2403940995751));
#8741=CARTESIAN_POINT('Ctrl Pts',(-20.562546663013,24.7584462352803,-68.2404530574361));
#8742=CARTESIAN_POINT('Ctrl Pts',(-20.5610880273173,24.7548362996531,-68.2407063945501));
#8743=CARTESIAN_POINT('Ctrl Pts',(-20.5599726175589,24.7520647148134,-68.2409006301762));
#8744=CARTESIAN_POINT('Ctrl Pts',(-20.5568346564899,24.7442360539812,-68.2414485074656));
#8745=CARTESIAN_POINT('Ctrl Pts',(-20.5548210592668,24.7391753726937,-68.2418017733164));
#8746=CARTESIAN_POINT('Ctrl Pts',(-20.5519319034874,24.7318602591712,-68.2423110919702));
#8747=CARTESIAN_POINT('Ctrl Pts',(-20.5510460485315,24.7296099340909,-68.2424675919954));
#8748=CARTESIAN_POINT('Ctrl Pts',(-20.5333523014502,24.6845138876407,-68.2456001856944));
#8749=CARTESIAN_POINT('Ctrl Pts',(-20.51746050167,24.6413111342092,-68.2485356299763));
#8750=CARTESIAN_POINT('Ctrl Pts',(-20.5008775199454,24.5930633849036,-68.2517301857399));
#8751=CARTESIAN_POINT('Ctrl Pts',(-20.4992673076188,24.5883428943877,-68.2520418563191));
#8752=CARTESIAN_POINT('Ctrl Pts',(-20.4968778044284,24.5812842534532,-68.2525065690145));
#8753=CARTESIAN_POINT('Ctrl Pts',(-20.4960902362059,24.5789489442941,-68.2526600985484));
#8754=CARTESIAN_POINT('Ctrl Pts',(-20.4947395977771,24.5749287873382,-68.252924016909));
#8755=CARTESIAN_POINT('Ctrl Pts',(-20.4941752419335,24.5732443778296,-68.2530344823545));
#8756=CARTESIAN_POINT('Ctrl Pts',(-20.4930108308903,24.5697594454971,-68.2532627911486));
#8757=CARTESIAN_POINT('Ctrl Pts',(-20.4924109745079,24.567958862413,-68.2533806220496));
#8758=CARTESIAN_POINT('Ctrl Pts',(-20.4910038265747,24.5637225643674,-68.2536575413108));
#8759=CARTESIAN_POINT('Ctrl Pts',(-20.4901978506868,24.5612864066244,-68.253816551057));
#8760=CARTESIAN_POINT('Ctrl Pts',(-20.4875792069138,24.5533394286967,-68.2543344895819));
#8761=CARTESIAN_POINT('Ctrl Pts',(-20.4857784959072,24.5478246355987,-68.254692711441));
#8762=CARTESIAN_POINT('Ctrl Pts',(-20.4186855997601,24.3404522742705,-68.2681188838046));
#8763=CARTESIAN_POINT('Ctrl Pts',(-20.3734578409923,24.1326053723328,-68.280027200704));
#8764=CARTESIAN_POINT('Ctrl Pts',(-20.3258451910703,23.7223625712184,-68.3031225818594));
#8765=CARTESIAN_POINT('Ctrl Pts',(-20.3213866639944,23.5212244485327,-68.3142748694118));
#8766=CARTESIAN_POINT('Ctrl Pts',(-20.3425413127634,23.2246130715782,-68.3316004063359));
#8767=CARTESIAN_POINT('Ctrl Pts',(-20.3537442694885,23.1286076444589,-68.3373402087703));
#8768=CARTESIAN_POINT('Ctrl Pts',(-20.3707324812254,23.0240812403174,-68.3437862229456));
#8769=CARTESIAN_POINT('Ctrl Pts',(-20.3722634424237,23.0149121494745,-68.3443533225711));
#8770=CARTESIAN_POINT('Ctrl Pts',(-20.3745964408629,23.0013023361239,-68.345197576675));
#8771=CARTESIAN_POINT('Ctrl Pts',(-20.3753681782888,22.9968564108051,-68.3454737664673));
#8772=CARTESIAN_POINT('Ctrl Pts',(-20.3767057401221,22.9892457044706,-68.345947243892));
#8773=CARTESIAN_POINT('Ctrl Pts',(-20.3772669690588,22.9860801132935,-68.3461443848693));
#8774=CARTESIAN_POINT('Ctrl Pts',(-20.3784154786972,22.9796579101137,-68.3465447498011));
#8775=CARTESIAN_POINT('Ctrl Pts',(-20.3790030401019,22.9764013533479,-68.3467479824616));
#8776=CARTESIAN_POINT('Ctrl Pts',(-20.3803640400305,22.9689239440949,-68.3472151267567));
#8777=CARTESIAN_POINT('Ctrl Pts',(-20.3811408938465,22.9647037267973,-68.3474791471202));
#8778=CARTESIAN_POINT('Ctrl Pts',(-20.3827875023543,22.9558578788056,-68.3480333238869));
#8779=CARTESIAN_POINT('Ctrl Pts',(-20.3836589656437,22.9512325799867,-68.3483235343973));
#8780=CARTESIAN_POINT('Ctrl Pts',(-20.3859874236818,22.9390213495532,-68.3490908981324));
#8781=CARTESIAN_POINT('Ctrl Pts',(-20.3874615589543,22.931438752846,-68.3495685989714));
#8782=CARTESIAN_POINT('Ctrl Pts',(-20.3919605925668,22.9087328881181,-68.3510027082182));
#8783=CARTESIAN_POINT('Ctrl Pts',(-20.3950667726421,22.893626124683,-68.3519617135873));
#8784=CARTESIAN_POINT('Ctrl Pts',(-20.4064383043499,22.8402656905905,-68.3553666407485));
#8785=CARTESIAN_POINT('Ctrl Pts',(-20.4152916358423,22.8021421288071,-68.3578312748854));
#8786=CARTESIAN_POINT('Ctrl Pts',(-20.4457042291217,22.6812203666782,-68.365753694121));
#8787=CARTESIAN_POINT('Ctrl Pts',(-20.4698656914929,22.5991206390235,-68.3712919623326));
#8788=CARTESIAN_POINT('Ctrl Pts',(-20.5499603288698,22.3622132927529,-68.3877335317863));
#8789=CARTESIAN_POINT('Ctrl Pts',(-20.6145137805871,22.2106182357555,-68.3988578573489));
#8790=CARTESIAN_POINT('Ctrl Pts',(-20.7666508900472,21.917746735208,-68.4211959001607));
#8791=CARTESIAN_POINT('Ctrl Pts',(-20.8541601935616,21.7769478307404,-68.4323745731446));
#8792=CARTESIAN_POINT('Ctrl Pts',(-20.974937338046,21.6123778985137,-68.4455118522025));
#8793=CARTESIAN_POINT('Ctrl Pts',(-20.9983251876517,21.5816810694138,-68.4479649473576));
#8794=CARTESIAN_POINT('Ctrl Pts',(-21.0252042376177,21.5476863756114,-68.4506776774405));
#8795=CARTESIAN_POINT('Ctrl Pts',(-21.0281567360848,21.5439691779872,-68.4509742509853));
#8796=CARTESIAN_POINT('Ctrl Pts',(-21.0326167201244,21.5383794588241,-68.4514201233923));
#8797=CARTESIAN_POINT('Ctrl Pts',(-21.0341180887413,21.5365020987663,-68.4515698570223));
#8798=CARTESIAN_POINT('Ctrl Pts',(-21.0367226814265,21.533252691861,-68.4518289899099));
#8799=CARTESIAN_POINT('Ctrl Pts',(-21.0378249290585,21.5318798694678,-68.4519384595416));
#8800=CARTESIAN_POINT('Ctrl Pts',(-21.0401246031371,21.5290204845374,-68.4521664466848));
#8801=CARTESIAN_POINT('Ctrl Pts',(-21.0413222241621,21.5275340841239,-68.4522849492619));
#8802=CARTESIAN_POINT('Ctrl Pts',(-21.0441724463008,21.524003020946,-68.4525664341196));
#8803=CARTESIAN_POINT('Ctrl Pts',(-21.0458262349608,21.5219593086712,-68.4527293302929));
#8804=CARTESIAN_POINT('Ctrl Pts',(-21.0513605804057,21.5151371860563,-68.4532730299902));
#8805=CARTESIAN_POINT('Ctrl Pts',(-21.0552523573808,21.5103678325207,-68.4536530250435));
#8806=CARTESIAN_POINT('Ctrl Pts',(-21.1643257927368,21.3774779982382,-68.4642389047057));
#8807=CARTESIAN_POINT('Ctrl Pts',(-21.2792406652269,21.2576299934558,-68.4737381390724));
#8808=CARTESIAN_POINT('Ctrl Pts',(-21.503742417469,21.05702005893,-68.4906942176977));
#8809=CARTESIAN_POINT('Ctrl Pts',(-21.6101728185252,20.9733351545359,-68.4981885093841));
#8810=CARTESIAN_POINT('Ctrl Pts',(-21.8898580130681,20.7805974719578,-68.517296381042));
#8811=CARTESIAN_POINT('Ctrl Pts',(-22.06879364077,20.6809042414171,-68.5290393120136));
#8812=CARTESIAN_POINT('Ctrl Pts',(-22.2674753949123,20.5937750939409,-68.5422224733009));
#8813=CARTESIAN_POINT('Ctrl Pts',(-22.2790330690148,20.5887871692002,-68.5429896914775));
#8814=CARTESIAN_POINT('Ctrl Pts',(-22.2948699439409,20.5820622675187,-68.5440415195785));
#8815=CARTESIAN_POINT('Ctrl Pts',(-22.2991242025228,20.5802665402181,-68.5443241259523));
#8816=CARTESIAN_POINT('Ctrl Pts',(-22.3063732979,20.5772250284158,-68.544805773771));
#8817=CARTESIAN_POINT('Ctrl Pts',(-22.3093661920335,20.5759746066437,-68.5450046572192));
#8818=CARTESIAN_POINT('Ctrl Pts',(-22.3154090021421,20.5734606480455,-68.5454062723513));
#8819=CARTESIAN_POINT('Ctrl Pts',(-22.3184589811948,20.5721972753473,-68.5456090092766));
#8820=CARTESIAN_POINT('Ctrl Pts',(-22.3254077356022,20.5693314397561,-68.5460709754418));
#8821=CARTESIAN_POINT('Ctrl Pts',(-22.3293077184872,20.5677319376818,-68.5463303047418));
#8822=CARTESIAN_POINT('Ctrl Pts',(-22.3374715151494,20.5644024112861,-68.5468732679235));
#8823=CARTESIAN_POINT('Ctrl Pts',(-22.3417359156785,20.5626738592416,-68.5471569510526));
#8824=CARTESIAN_POINT('Ctrl Pts',(-22.3529355154231,20.5581620637123,-68.5479021623777));
#8825=CARTESIAN_POINT('Ctrl Pts',(-22.3598766890141,20.5553938108705,-68.548364196654));
#8826=CARTESIAN_POINT('Ctrl Pts',(-22.3805403578621,20.5472359903918,-68.5497402114108));
#8827=CARTESIAN_POINT('Ctrl Pts',(-22.3942901341515,20.5419164732122,-68.5506565461458));
#8828=CARTESIAN_POINT('Ctrl Pts',(-22.4425200121628,20.5236367544383,-68.5538735445131));
#8829=CARTESIAN_POINT('Ctrl Pts',(-22.4771843559801,20.5111739037259,-68.5561907015506));
#8830=CARTESIAN_POINT('Ctrl Pts',(-22.6398817883655,20.4558099594653,-68.5670930000249));
#8831=CARTESIAN_POINT('Ctrl Pts',(-22.7703015498735,20.4203933879633,-68.5759170084932));
#8832=CARTESIAN_POINT('Ctrl Pts',(-23.2052705149168,20.3311523784487,-68.6055192030266));
#8833=CARTESIAN_POINT('Ctrl Pts',(-23.5153440177527,20.3129078258319,-68.6270450846501));
#8834=CARTESIAN_POINT('Ctrl Pts',(-23.8394162639224,20.340460546158,-68.6476283576837));
#8835=CARTESIAN_POINT('Ctrl Pts',(-23.8555555941309,20.3419554256334,-68.648647921971));
#8836=CARTESIAN_POINT('Ctrl Pts',(-23.8752514992914,20.3439297012358,-68.6498848579311));
#8837=CARTESIAN_POINT('Ctrl Pts',(-23.8788190629481,20.3442933215815,-68.650108613836));
#8838=CARTESIAN_POINT('Ctrl Pts',(-23.884698784567,20.3449025238657,-68.650476895652));
#8839=CARTESIAN_POINT('Ctrl Pts',(-23.8870112839392,20.3451446533843,-68.6506216158127));
#8840=CARTESIAN_POINT('Ctrl Pts',(-23.8911800749013,20.3455857068698,-68.6508822772995));
#8841=CARTESIAN_POINT('Ctrl Pts',(-23.8930364512133,20.3457837407047,-68.6509982688233));
#8842=CARTESIAN_POINT('Ctrl Pts',(-23.8970276598182,20.3462130213372,-68.6512474741189));
#8843=CARTESIAN_POINT('Ctrl Pts',(-23.8991624274529,20.3464447880678,-68.6513806576683));
#8844=CARTESIAN_POINT('Ctrl Pts',(-23.9050075792497,20.3470852939922,-68.6517450315093));
#8845=CARTESIAN_POINT('Ctrl Pts',(-23.9087175022022,20.3474983479163,-68.6519759770003));
#8846=CARTESIAN_POINT('Ctrl Pts',(-23.9279704133344,20.3496757928681,-68.6531728476588));
#8847=CARTESIAN_POINT('Ctrl Pts',(-23.9435014714727,20.3515469256761,-68.6541328055749));
#8848=CARTESIAN_POINT('Ctrl Pts',(-24.0947402592146,20.3708858937837,-68.6634320301399));
#8849=CARTESIAN_POINT('Ctrl Pts',(-24.2292376413564,20.396868924638,-68.6713217829587));
#8850=CARTESIAN_POINT('Ctrl Pts',(-24.4935588054859,20.4656363564986,-68.6867741515009));
#8851=CARTESIAN_POINT('Ctrl Pts',(-24.623120246657,20.5082729018273,-68.6943245275661));
#8852=CARTESIAN_POINT('Ctrl Pts',(-24.8248664953339,20.5891626547212,-68.7065177793488));
#8853=CARTESIAN_POINT('Ctrl Pts',(-24.8989685371041,20.6221715338371,-68.7110943476401));
#8854=CARTESIAN_POINT('Ctrl Pts',(-25.0987337267806,20.7203505797276,-68.7238389289412));
#8855=CARTESIAN_POINT('Ctrl Pts',(-25.2214590024225,20.7910497539876,-68.7321352727002));
#8856=CARTESIAN_POINT('Ctrl Pts',(-25.3483324759706,20.875715486634,-68.7414135918751));
#8857=CARTESIAN_POINT('Ctrl Pts',(-25.3575006022925,20.8819020491041,-68.7420881477478));
#8858=CARTESIAN_POINT('Ctrl Pts',(-25.3702462124476,20.8905984828731,-68.743031709413));
#8859=CARTESIAN_POINT('Ctrl Pts',(-25.3738507857663,20.8930686718847,-68.7432992070227));
#8860=CARTESIAN_POINT('Ctrl Pts',(-25.3800673735743,20.8973474635477,-68.7437616725831));
#8861=CARTESIAN_POINT('Ctrl Pts',(-25.3826817650288,20.8991526163998,-68.7439565088454));
#8862=CARTESIAN_POINT('Ctrl Pts',(-25.3880320204405,20.9028584901966,-68.7443559456217));
#8863=CARTESIAN_POINT('Ctrl Pts',(-25.3907676139811,20.9047595923806,-68.7445605605388));
#8864=CARTESIAN_POINT('Ctrl Pts',(-25.3971215476363,20.909189887663,-68.7450367099658));
#8865=CARTESIAN_POINT('Ctrl Pts',(-25.4007376418388,20.9117222763119,-68.7453083667574));
#8866=CARTESIAN_POINT('Ctrl Pts',(-25.4083378075222,20.9170680606944,-68.745880752323));
#8867=CARTESIAN_POINT('Ctrl Pts',(-25.412320715415,20.9198830843885,-68.7461815433369));
#8868=CARTESIAN_POINT('Ctrl Pts',(-25.4229293130872,20.9274171567157,-68.746984934149));
#8869=CARTESIAN_POINT('Ctrl Pts',(-25.4295435199946,20.9321522450075,-68.7474881525465));
#8870=CARTESIAN_POINT('Ctrl Pts',(-25.4495553366796,20.9465935440393,-68.7490177915468));
#8871=CARTESIAN_POINT('Ctrl Pts',(-25.4628960384992,20.9563778106588,-68.7500472358163));
#8872=CARTESIAN_POINT('Ctrl Pts',(-25.7200367833645,21.148030937166,-68.77008120539));
#8873=CARTESIAN_POINT('Ctrl Pts',(-25.9369016867115,21.3633708285556,-68.7905582849646));
#8874=CARTESIAN_POINT('Ctrl Pts',(-26.2033160982451,21.7155075814947,-68.8204211139728));
#8875=CARTESIAN_POINT('Ctrl Pts',(-26.2792015973723,21.8304040920889,-68.8296738478804));
#8876=CARTESIAN_POINT('Ctrl Pts',(-26.35241433982,21.9583656029755,-68.8392272503183));
#8877=CARTESIAN_POINT('Ctrl Pts',(-26.3572719241504,21.9669468354047,-68.8398644128024));
#8878=CARTESIAN_POINT('Ctrl Pts',(-26.3816676333692,22.0105085779592,-68.8430807304864));
#8879=CARTESIAN_POINT('Ctrl Pts',(-26.4005926756583,22.0458309307211,-68.8456296287692));
#8880=CARTESIAN_POINT('Ctrl Pts',(-26.4212837676865,22.0862424214369,-68.8484717083514));
#8881=CARTESIAN_POINT('Ctrl Pts',(-26.4237006969254,22.0909918957284,-68.8488045865178));
#8882=CARTESIAN_POINT('Ctrl Pts',(-26.427212286108,22.0979350237288,-68.8492895179026));
#8883=CARTESIAN_POINT('Ctrl Pts',(-26.4283162251884,22.1001239343809,-68.8494421535204));
#8884=CARTESIAN_POINT('Ctrl Pts',(-26.4302652229485,22.1039994351109,-68.8497119606848));
#8885=CARTESIAN_POINT('Ctrl Pts',(-26.4311112989708,22.1056855085893,-68.8498291967788));
#8886=CARTESIAN_POINT('Ctrl Pts',(-26.4328740508249,22.1092060558736,-68.8500736817176));
#8887=CARTESIAN_POINT('Ctrl Pts',(-26.4337904542976,22.1110406581345,-68.8502009131364));
#8888=CARTESIAN_POINT('Ctrl Pts',(-26.4361773434937,22.1158305438829,-68.8505326487636));
#8889=CARTESIAN_POINT('Ctrl Pts',(-26.4376450458078,22.1187872236447,-68.8507369769917));
#8890=CARTESIAN_POINT('Ctrl Pts',(-26.4439862228812,22.1316109294938,-68.8516212882347));
#8891=CARTESIAN_POINT('Ctrl Pts',(-26.4488137577405,22.1415007799124,-68.8522984124451));
#8892=CARTESIAN_POINT('Ctrl Pts',(-26.4833267153623,22.2131336936917,-68.8571691534399));
#8893=CARTESIAN_POINT('Ctrl Pts',(-26.5110898137452,22.2757898494736,-68.8612491846057));
#8894=CARTESIAN_POINT('Ctrl Pts',(-26.6927522813078,22.7238215175353,-68.8894944968044));
#8895=CARTESIAN_POINT('Ctrl Pts',(-26.7729452984221,23.1348231300911,-68.9111907440968));
#8896=CARTESIAN_POINT('Ctrl Pts',(-26.7730025010771,23.5498082993017,-68.9362096369654));
#8897=CARTESIAN_POINT('Ctrl Pts',(-26.7730025012977,23.5498099025822,-68.936209733625));
#8898=CARTESIAN_POINT('Ctrl Pts',(-26.7730047857272,23.5664426653496,-68.9372125005807));
#8899=CARTESIAN_POINT('Ctrl Pts',(-26.772878306465,23.58307501592,-68.9382191818676));
#8900=CARTESIAN_POINT('Ctrl Pts',(-26.7724443818348,23.6113496939998,-68.9399375387905));
#8901=CARTESIAN_POINT('Ctrl Pts',(-26.7722025683611,23.6229927406453,-68.9406471532271));
#8902=CARTESIAN_POINT('Ctrl Pts',(-26.7717888541505,23.6387881371692,-68.9416126668269));
#8903=CARTESIAN_POINT('Ctrl Pts',(-26.7716720174634,23.6429419420569,-68.9418668383947));
#8904=CARTESIAN_POINT('Ctrl Pts',(-26.7714493519704,23.6503484808087,-68.9423205218401));
#8905=CARTESIAN_POINT('Ctrl Pts',(-26.7713466290917,23.6536013080502,-68.942519936029));
#8906=CARTESIAN_POINT('Ctrl Pts',(-26.7711312513569,23.6601089951004,-68.9429192195149));
#8907=CARTESIAN_POINT('Ctrl Pts',(-26.7710185894345,23.6633638508018,-68.9431190888013));
#8908=CARTESIAN_POINT('Ctrl Pts',(-26.7707837590673,23.6698632246213,-68.9435185251654));
#8909=CARTESIAN_POINT('Ctrl Pts',(-26.7706616209194,23.6731077402234,-68.9437180910701));
#8910=CARTESIAN_POINT('Ctrl Pts',(-26.7703162116814,23.6819286709191,-68.9442611079359));
#8911=CARTESIAN_POINT('Ctrl Pts',(-26.7700833589032,23.6875046804617,-68.9446048596047));
#8912=CARTESIAN_POINT('Ctrl Pts',(-26.7691540744085,23.7084523906252,-68.9458981199291));
#8913=CARTESIAN_POINT('Ctrl Pts',(-26.7683620463268,23.723819451571,-68.9468506280402));
#8914=CARTESIAN_POINT('Ctrl Pts',(-26.7662646518848,23.7595355479009,-68.9490734664427));
#8915=CARTESIAN_POINT('Ctrl Pts',(-26.7648761573847,23.7798788637678,-68.9503463773295));
#8916=CARTESIAN_POINT('Ctrl Pts',(-26.7353843105202,24.1589817036011,-68.9741978283998));
#8917=CARTESIAN_POINT('Ctrl Pts',(-26.6475757806062,24.5104963231395,-68.9989194497197));
#8918=CARTESIAN_POINT('Ctrl Pts',(-26.4844888954227,24.8839168194867,-69.0261657804982));
#8919=CARTESIAN_POINT('Ctrl Pts',(-26.4643798809675,24.9273021383577,-69.0293406201353));
#8920=CARTESIAN_POINT('Ctrl Pts',(-26.4133699584253,25.0312299947696,-69.0369436560686));
#8921=CARTESIAN_POINT('Ctrl Pts',(-26.3815029812796,25.0912775542513,-69.0413348146074));
#8922=CARTESIAN_POINT('Ctrl Pts',(-26.3423214543282,25.159783088812,-69.0463045707472));
#8923=CARTESIAN_POINT('Ctrl Pts',(-26.3368361010281,25.1692613341405,-69.0469912584852));
#8924=CARTESIAN_POINT('Ctrl Pts',(-26.329637524234,25.1815549200339,-69.0478805348423));
#8925=CARTESIAN_POINT('Ctrl Pts',(-26.3279682322108,25.1843957036023,-69.0480859312124));
#8926=CARTESIAN_POINT('Ctrl Pts',(-26.3252535946822,25.1889992671449,-69.0484186186806));
#8927=CARTESIAN_POINT('Ctrl Pts',(-26.3242109246451,25.1907636096113,-69.0485460842482));
#8928=CARTESIAN_POINT('Ctrl Pts',(-26.322205030417,25.1941504809885,-69.048790693558));
#8929=CARTESIAN_POINT('Ctrl Pts',(-26.3212420670504,25.1957731538166,-69.0489078535295));
#8930=CARTESIAN_POINT('Ctrl Pts',(-26.3190232345048,25.1995045991043,-69.0491771942288));
#8931=CARTESIAN_POINT('Ctrl Pts',(-26.3177663779144,25.2016127884749,-69.0493293099522));
#8932=CARTESIAN_POINT('Ctrl Pts',(-26.3137651341339,25.2083068796249,-69.049812148015));
#8933=CARTESIAN_POINT('Ctrl Pts',(-26.311011729127,25.2128874222515,-69.0501422812382));
#8934=CARTESIAN_POINT('Ctrl Pts',(-26.2873084037128,25.2520988552947,-69.0529663493015));
#8935=CARTESIAN_POINT('Ctrl Pts',(-26.2657180274317,25.2863410285963,-69.0554190226764));
#8936=CARTESIAN_POINT('Ctrl Pts',(-26.2376568933535,25.3290408991718,-69.0584722976328));
#8937=CARTESIAN_POINT('Ctrl Pts',(-26.2317828376824,25.3378837808995,-69.0591043250443));
#8938=CARTESIAN_POINT('Ctrl Pts',(-26.2240361610296,25.349421626437,-69.0599288163941));
#8939=CARTESIAN_POINT('Ctrl Pts',(-26.222203036043,25.3521428808695,-69.0601232652824));
#8940=CARTESIAN_POINT('Ctrl Pts',(-26.2187551941726,25.3572443344973,-69.0604877811128));
#8941=CARTESIAN_POINT('Ctrl Pts',(-26.2171414421803,25.3596251782998,-69.0606578955518));
#8942=CARTESIAN_POINT('Ctrl Pts',(-26.0677040316585,25.5794629306854,-69.0763654654895));
#8943=CARTESIAN_POINT('Ctrl Pts',(-25.8938104024267,25.7780376692195,-69.0906110560752));
#8944=CARTESIAN_POINT('Ctrl Pts',(-25.5954822153969,26.0446353437266,-69.1132057281776));
#8945=CARTESIAN_POINT('Ctrl Pts',(-25.4875506000165,26.1293571049431,-69.1210744989442));
#8946=CARTESIAN_POINT('Ctrl Pts',(-25.3439069814071,26.2279948667579,-69.1314210853924));
#8947=CARTESIAN_POINT('Ctrl Pts',(-25.3128921676622,26.24851153353,-69.1336475276948));
#8948=CARTESIAN_POINT('Ctrl Pts',(-25.269007453273,26.2764622663053,-69.1367908814048));
#8949=CARTESIAN_POINT('Ctrl Pts',(-25.256429878296,26.2843514414055,-69.1376909897331));
#8950=CARTESIAN_POINT('Ctrl Pts',(-25.2374075927188,26.2961006313164,-69.1390513196822));
#8951=CARTESIAN_POINT('Ctrl Pts',(-25.2310030480904,26.3000255561954,-69.1395091562692));
#8952=CARTESIAN_POINT('Ctrl Pts',(-25.2206393462675,26.306327054413,-69.1402497722269));
#8953=CARTESIAN_POINT('Ctrl Pts',(-25.2166886749389,26.3087175877024,-69.1405320396322));
#8954=CARTESIAN_POINT('Ctrl Pts',(-25.2091127943546,26.3132795037896,-69.1410732175398));
#8955=CARTESIAN_POINT('Ctrl Pts',(-25.2054884228306,26.315452264803,-69.1413320769522));
#8956=CARTESIAN_POINT('Ctrl Pts',(-25.1990235922908,26.3193105775899,-69.1417937314407));
#8957=CARTESIAN_POINT('Ctrl Pts',(-25.1961847904749,26.3209989060804,-69.1419964247152));
#8958=CARTESIAN_POINT('Ctrl Pts',(-25.1905571631761,26.3243341397778,-69.1423981937817));
#8959=CARTESIAN_POINT('Ctrl Pts',(-25.1877684400636,26.3259812111722,-69.1425972632179));
#8960=CARTESIAN_POINT('Ctrl Pts',(-25.1810127965991,26.3299574949305,-69.1430794511156));
#8961=CARTESIAN_POINT('Ctrl Pts',(-25.1770433707906,26.3322824182561,-69.14336272528));
#8962=CARTESIAN_POINT('Ctrl Pts',(-25.1622908936194,26.3408806888472,-69.1444153619796));
#8963=CARTESIAN_POINT('Ctrl Pts',(-25.151476530137,26.3470998445792,-69.1451866869078));
#8964=CARTESIAN_POINT('Ctrl Pts',(-24.9649559844927,26.4529282590483,-69.1584856072429));
#8965=CARTESIAN_POINT('Ctrl Pts',(-24.7803397180759,26.5358462630855,-69.1716245620863));
#8966=CARTESIAN_POINT('Ctrl Pts',(-24.496742596601,26.6324297467823,-69.1916844879187));
#8967=CARTESIAN_POINT('Ctrl Pts',(-24.4028920249507,26.6597001777809,-69.1982960438932));
#8968=CARTESIAN_POINT('Ctrl Pts',(-24.2788949017737,26.6896938055823,-69.2069313823461));
#8969=CARTESIAN_POINT('Ctrl Pts',(-24.2497423287454,26.6963175745166,-69.2089543340347));
#8970=CARTESIAN_POINT('Ctrl Pts',(-24.127174113375,26.722378453355,-69.2174211347823));
#8971=CARTESIAN_POINT('Ctrl Pts',(-24.0330060972836,26.7380687610298,-69.2238343968652));
#8972=CARTESIAN_POINT('Ctrl Pts',(-23.8826539866267,26.7563040246646,-69.2338096230969));
#8973=CARTESIAN_POINT('Ctrl Pts',(-23.8268615332397,26.7615988515387,-69.2374537281834));
#8974=CARTESIAN_POINT('Ctrl Pts',(-23.743803416906,26.7673003010701,-69.242766835119));
#8975=CARTESIAN_POINT('Ctrl Pts',(-23.7166272603371,26.7688202047084,-69.244487504083));
#8976=CARTESIAN_POINT('Ctrl Pts',(-23.6850418372695,26.7701855640726,-69.2464642176118));
#8977=CARTESIAN_POINT('Ctrl Pts',(-23.6806492301382,26.7703664414001,-69.2467386012553));
#8978=CARTESIAN_POINT('Ctrl Pts',(-23.6739669273225,26.7706279072942,-69.2471552064107));
#8979=CARTESIAN_POINT('Ctrl Pts',(-23.6716775155677,26.7707150427051,-69.247297795218));
#8980=CARTESIAN_POINT('Ctrl Pts',(-23.6675245464164,26.770868670617,-69.2475561870839));
#8981=CARTESIAN_POINT('Ctrl Pts',(-23.6656610302617,26.7709359868383,-69.2476720362983));
#8982=CARTESIAN_POINT('Ctrl Pts',(-23.6616254011732,26.7710782596815,-69.2479227109524));
#8983=CARTESIAN_POINT('Ctrl Pts',(-23.6594532765641,26.771152636247,-69.2480575029532));
#8984=CARTESIAN_POINT('Ctrl Pts',(-23.6535334272755,26.7713493448072,-69.2484245101867));
#8985=CARTESIAN_POINT('Ctrl Pts',(-23.6497855468011,26.7714673339204,-69.2486564803599));
#8986=CARTESIAN_POINT('Ctrl Pts',(-23.6318357024983,26.7720010657349,-69.2497656619702));
#8987=CARTESIAN_POINT('Ctrl Pts',(-23.6176310121315,26.7723294377139,-69.2506380202415));
#8988=CARTESIAN_POINT('Ctrl Pts',(-23.5942080303515,26.7727159433589,-69.252068288187));
#8989=CARTESIAN_POINT('Ctrl Pts',(-23.5849910218605,26.7728284838172,-69.2526290054951));
#8990=CARTESIAN_POINT('Ctrl Pts',(-23.5707753235361,26.7729410616666,-69.2534907581141));
#8991=CARTESIAN_POINT('Ctrl Pts',(-23.5657769920613,26.7729690159653,-69.2537931724743));
#8992=CARTESIAN_POINT('Ctrl Pts',(-23.5565209192551,26.7729992480387,-69.2543521460652));
#8993=CARTESIAN_POINT('Ctrl Pts',(-23.5522632081041,26.7730047170143,-69.2546088586567));
#8994=CARTESIAN_POINT('Ctrl Pts',(-23.2600292273571,26.772800957288,-69.2722012879213));
#8995=CARTESIAN_POINT('Ctrl Pts',(-22.9733344466731,26.7340030985608,-69.2877244865341));
#8996=CARTESIAN_POINT('Ctrl Pts',(-22.5776010697416,26.625157151951,-69.3108910344547));
#8997=CARTESIAN_POINT('Ctrl Pts',(-22.461576891171,26.5860177755781,-69.3178958131221));
#8998=CARTESIAN_POINT('Ctrl Pts',(-22.3032582707111,26.5223654272652,-69.3279515706952));
#8999=CARTESIAN_POINT('Ctrl Pts',(-22.2588638310277,26.5033466058835,-69.3308274326826));
#9000=CARTESIAN_POINT('Ctrl Pts',(-22.198504047799,26.4758667824886,-69.3348232483214));
#9001=CARTESIAN_POINT('Ctrl Pts',(-22.1821562272589,26.468257876046,-69.3359142481335));
#9002=CARTESIAN_POINT('Ctrl Pts',(-22.1580452288087,26.4567885343138,-69.3375367370518));
#9003=CARTESIAN_POINT('Ctrl Pts',(-22.1502322029151,26.453033230514,-69.3380645944178));
#9004=CARTESIAN_POINT('Ctrl Pts',(-22.1378485580156,26.4470194481036,-69.3389046270686));
#9005=CARTESIAN_POINT('Ctrl Pts',(-22.133267945313,26.4447815494024,-69.3392160858091));
#9006=CARTESIAN_POINT('Ctrl Pts',(-22.124588497545,26.4405155885311,-69.3398076538194));
#9007=CARTESIAN_POINT('Ctrl Pts',(-22.1204886276497,26.4384896504801,-69.3400876883751));
#9008=CARTESIAN_POINT('Ctrl Pts',(-22.1133852226176,26.4349606935177,-69.3405739186372));
#9009=CARTESIAN_POINT('Ctrl Pts',(-22.110379691644,26.4334616894092,-69.3407799732988));
#9010=CARTESIAN_POINT('Ctrl Pts',(-22.1045714964856,26.4305535138229,-69.3411788060404));
#9011=CARTESIAN_POINT('Ctrl Pts',(-22.1017685344648,26.4291449424779,-69.3413715628621));
#9012=CARTESIAN_POINT('Ctrl Pts',(-22.0952060469638,26.4258350881028,-69.341823529226));
#9013=CARTESIAN_POINT('Ctrl Pts',(-22.0914481903326,26.4239305242344,-69.342082854101));
#9014=CARTESIAN_POINT('Ctrl Pts',(-22.0834699473044,26.4198672940224,-69.3426345265533));
#9015=CARTESIAN_POINT('Ctrl Pts',(-22.0792505779957,26.4177066787971,-69.3429269421883));
#9016=CARTESIAN_POINT('Ctrl Pts',(-22.075036015343,26.4155367745547,-69.3432196869019));
#9017=CARTESIAN_POINT('',(-26.7730011432084,23.5532287591033,-69.1857955693508));
#9018=CARTESIAN_POINT('Ctrl Pts',(-22.0750360905742,26.4155368132881,-69.5918437005959));
#9019=CARTESIAN_POINT('Ctrl Pts',(-22.1526654206688,26.455504946574,-69.5869494799723));
#9020=CARTESIAN_POINT('Ctrl Pts',(-22.2319114232218,26.4923143489673,-69.5820862962769));
#9021=CARTESIAN_POINT('Ctrl Pts',(-22.44915197364,26.5826729369313,-69.5689009104334));
#9022=CARTESIAN_POINT('Ctrl Pts',(-22.5894619030909,26.630004415548,-69.5605298696121));
#9023=CARTESIAN_POINT('Ctrl Pts',(-22.7520381357013,26.6726520380195,-69.5506819137278));
#9024=CARTESIAN_POINT('Ctrl Pts',(-22.7716075670712,26.6775895607603,-69.5494943265321));
#9025=CARTESIAN_POINT('Ctrl Pts',(-22.7959524371243,26.6834892963067,-69.548013626738));
#9026=CARTESIAN_POINT('Ctrl Pts',(-22.8006856549551,26.6846249972324,-69.5477255891229));
#9027=CARTESIAN_POINT('Ctrl Pts',(-22.8093737704392,26.6866888416268,-69.5471965828521));
#9028=CARTESIAN_POINT('Ctrl Pts',(-22.8133278900566,26.6876202400569,-69.5469557104002));
#9029=CARTESIAN_POINT('Ctrl Pts',(-22.8230998256346,26.6899025403004,-69.5463601492596));
#9030=CARTESIAN_POINT('Ctrl Pts',(-22.8289196406151,26.6912447465899,-69.5460052044055));
#9031=CARTESIAN_POINT('Ctrl Pts',(-22.8414939534858,26.6941079318187,-69.5452377454647));
#9032=CARTESIAN_POINT('Ctrl Pts',(-22.8482496792331,26.6956233354519,-69.5448250666928));
#9033=CARTESIAN_POINT('Ctrl Pts',(-22.8627027654149,26.6988164814011,-69.5439414031395));
#9034=CARTESIAN_POINT('Ctrl Pts',(-22.8704014880375,26.7004877901034,-69.5434702268306));
#9035=CARTESIAN_POINT('Ctrl Pts',(-22.8975403951096,26.7062752332475,-69.5418075172284));
#9036=CARTESIAN_POINT('Ctrl Pts',(-22.9170121558457,26.7102397192776,-69.5406113725651));
#9037=CARTESIAN_POINT('Ctrl Pts',(-22.9563188402286,26.7178647425853,-69.5381896836691));
#9038=CARTESIAN_POINT('Ctrl Pts',(-22.9761539284892,26.7215196465053,-69.5369640228348));
#9039=CARTESIAN_POINT('Ctrl Pts',(-23.0021561750857,26.7260590001987,-69.535352138365));
#9040=CARTESIAN_POINT('Ctrl Pts',(-23.0082937346417,26.7271121450482,-69.5349712964485));
#9041=CARTESIAN_POINT('Ctrl Pts',(-23.0177639625179,26.7287089004688,-69.5343830707604));
#9042=CARTESIAN_POINT('Ctrl Pts',(-23.0210945210074,26.729265077139,-69.5341760871908));
#9043=CARTESIAN_POINT('Ctrl Pts',(-23.0277246209186,26.7303615430132,-69.5337638221453));
#9044=CARTESIAN_POINT('Ctrl Pts',(-23.0310241414461,26.730901933945,-69.533558544184));
#9045=CARTESIAN_POINT('Ctrl Pts',(-23.0383344573878,26.7320875290667,-69.5331034880886));
#9046=CARTESIAN_POINT('Ctrl Pts',(-23.0423456390098,26.7327302854936,-69.5328536324775));
#9047=CARTESIAN_POINT('Ctrl Pts',(-23.0506164299402,26.7340395718234,-69.5323381012382));
#9048=CARTESIAN_POINT('Ctrl Pts',(-23.0548761810921,26.7347051411775,-69.5320723955862));
#9049=CARTESIAN_POINT('Ctrl Pts',(-23.0773794142197,26.7381749375841,-69.5306677282192));
#9050=CARTESIAN_POINT('Ctrl Pts',(-23.0956451041122,26.7408308985702,-69.5295240683848));
#9051=CARTESIAN_POINT('Ctrl Pts',(-23.221749670685,26.7580625436592,-69.5216031247671));
#9052=CARTESIAN_POINT('Ctrl Pts',(-23.330232201697,26.7673235133517,-69.5146584174444));
#9053=CARTESIAN_POINT('Ctrl Pts',(-23.6038113319815,26.7767762877768,-69.4968017051579));
#9054=CARTESIAN_POINT('Ctrl Pts',(-23.768835155235,26.7698077088262,-69.4857073897485));
#9055=CARTESIAN_POINT('Ctrl Pts',(-24.1270260032621,26.7270114879794,-69.4612936574412));
#9056=CARTESIAN_POINT('Ctrl Pts',(-24.3189644709451,26.6861035175699,-69.447992579817));
#9057=CARTESIAN_POINT('Ctrl Pts',(-24.5091463157055,26.6270448588762,-69.4352497852357));
#9058=CARTESIAN_POINT('Ctrl Pts',(-24.5122762234432,26.626067664359,-69.4350402020583));
#9059=CARTESIAN_POINT('Ctrl Pts',(-24.5210231841025,26.6233221015398,-69.4344548688866));
#9060=CARTESIAN_POINT('Ctrl Pts',(-24.5266369232218,26.6215431011206,-69.434079640099));
#9061=CARTESIAN_POINT('Ctrl Pts',(-24.553136092147,26.6130654865465,-69.4323105602391));
#9062=CARTESIAN_POINT('Ctrl Pts',(-24.5739583129835,26.6061689522566,-69.4309268036991));
#9063=CARTESIAN_POINT('Ctrl Pts',(-24.5984792687022,26.5977685943256,-69.4293061008247));
#9064=CARTESIAN_POINT('Ctrl Pts',(-24.6022469825688,26.59647004197,-69.4290573235621));
#9065=CARTESIAN_POINT('Ctrl Pts',(-24.6083000377138,26.5943712712385,-69.4286580587353));
#9066=CARTESIAN_POINT('Ctrl Pts',(-24.6105868876512,26.5935754654476,-69.4285073104458));
#9067=CARTESIAN_POINT('Ctrl Pts',(-24.6146496443481,26.592156522811,-69.4282396655508));
#9068=CARTESIAN_POINT('Ctrl Pts',(-24.6164259025886,26.5915344074608,-69.4281227078813));
#9069=CARTESIAN_POINT('Ctrl Pts',(-24.6201505221503,26.5902262354033,-69.427877583209));
#9070=CARTESIAN_POINT('Ctrl Pts',(-24.6220987646433,26.5895398629934,-69.427749435716));
#9071=CARTESIAN_POINT('Ctrl Pts',(-24.6260552333066,26.5881417082894,-69.4274893354236));
#9072=CARTESIAN_POINT('Ctrl Pts',(-24.6280634165674,26.5874298064977,-69.4273573898581));
#9073=CARTESIAN_POINT('Ctrl Pts',(-24.6330271800261,26.5856646072229,-69.4270314292175));
#9074=CARTESIAN_POINT('Ctrl Pts',(-24.6359819386083,26.5846089811732,-69.4268375523524));
#9075=CARTESIAN_POINT('Ctrl Pts',(-24.6648192100615,26.5742589752997,-69.4249468751775));
#9076=CARTESIAN_POINT('Ctrl Pts',(-24.6905843284826,26.564637604443,-69.4232693009594));
#9077=CARTESIAN_POINT('Ctrl Pts',(-24.7720607432397,26.533017949571,-69.4179921267483));
#9078=CARTESIAN_POINT('Ctrl Pts',(-24.8272862343931,26.5097948496602,-69.4144568066649));
#9079=CARTESIAN_POINT('Ctrl Pts',(-24.9639619637344,26.4477818921222,-69.4057362316423));
#9080=CARTESIAN_POINT('Ctrl Pts',(-25.0444925043024,26.4070863494505,-69.400623844108));
#9081=CARTESIAN_POINT('Ctrl Pts',(-25.1955577619493,26.3226086699534,-69.3908958354119));
#9082=CARTESIAN_POINT('Ctrl Pts',(-25.2663145947021,26.2793767709488,-69.3862772145548));
#9083=CARTESIAN_POINT('Ctrl Pts',(-25.5386973541227,26.0981673361259,-69.3679811940941));
#9084=CARTESIAN_POINT('Ctrl Pts',(-25.7259934010847,25.9402126340196,-69.3541597507562));
#9085=CARTESIAN_POINT('Ctrl Pts',(-25.9039914836604,25.7516742872414,-69.3384289345038));
#9086=CARTESIAN_POINT('Ctrl Pts',(-25.9142627162647,25.7406407701064,-69.3375111215199));
#9087=CARTESIAN_POINT('Ctrl Pts',(-25.9281979548689,25.7254591305463,-69.3362518462503));
#9088=CARTESIAN_POINT('Ctrl Pts',(-25.9319293567771,25.7213729068797,-69.3359132575238));
#9089=CARTESIAN_POINT('Ctrl Pts',(-25.9378271949678,25.714880738044,-69.3353758576808));
#9090=CARTESIAN_POINT('Ctrl Pts',(-25.9400005734878,25.7124810906239,-69.3351773410354));
#9091=CARTESIAN_POINT('Ctrl Pts',(-25.9442035992433,25.7078264130088,-69.3347924978296));
#9092=CARTESIAN_POINT('Ctrl Pts',(-25.9462336862373,25.705571782786,-69.3346061901252));
#9093=CARTESIAN_POINT('Ctrl Pts',(-25.9510531905909,25.7002039803247,-69.3341628716662));
#9094=CARTESIAN_POINT('Ctrl Pts',(-25.9538397355973,25.6970882469265,-69.3339057403805));
#9095=CARTESIAN_POINT('Ctrl Pts',(-25.9595965152841,25.6906261326891,-69.333372836069));
#9096=CARTESIAN_POINT('Ctrl Pts',(-25.9625658568267,25.6872789714372,-69.3330970263072));
#9097=CARTESIAN_POINT('Ctrl Pts',(-25.9702752065525,25.678552140372,-69.3323784828483));
#9098=CARTESIAN_POINT('Ctrl Pts',(-25.9750042301088,25.6731628385201,-69.3319352909789));
#9099=CARTESIAN_POINT('Ctrl Pts',(-26.0162936474098,25.6257905378528,-69.328044312553));
#9100=CARTESIAN_POINT('Ctrl Pts',(-26.0517765300322,25.5828847805752,-69.3245522224528));
#9101=CARTESIAN_POINT('Ctrl Pts',(-26.164353259825,25.4393428558225,-69.3129623477816));
#9102=CARTESIAN_POINT('Ctrl Pts',(-26.2366162140843,25.3350854297851,-69.3046829454011));
#9103=CARTESIAN_POINT('Ctrl Pts',(-26.3256596253924,25.1889126025371,-69.2932871026055));
#9104=CARTESIAN_POINT('Ctrl Pts',(-26.3479849621949,25.1504976479136,-69.2903115574893));
#9105=CARTESIAN_POINT('Ctrl Pts',(-26.3913505825243,25.0721959883959,-69.2842918449286));
#9106=CARTESIAN_POINT('Ctrl Pts',(-26.4123623754852,25.0323042027475,-69.2812479509936));
#9107=CARTESIAN_POINT('Ctrl Pts',(-26.5341153268384,24.7888986226874,-69.2628410576715));
#9108=CARTESIAN_POINT('Ctrl Pts',(-26.6139622893896,24.5756233741797,-69.2473531455926));
#9109=CARTESIAN_POINT('Ctrl Pts',(-26.6741330520243,24.3425111998598,-69.2321513448168));
#9110=CARTESIAN_POINT('Ctrl Pts',(-26.6774555611289,24.3292933079112,-69.2312952252948));
#9111=CARTESIAN_POINT('Ctrl Pts',(-26.6815714281676,24.3124684852463,-69.2302132597225));
#9112=CARTESIAN_POINT('Ctrl Pts',(-26.6824425102604,24.3088809847302,-69.2299830039435));
#9113=CARTESIAN_POINT('Ctrl Pts',(-26.6838134769649,24.3031921243742,-69.2296185957857));
#9114=CARTESIAN_POINT('Ctrl Pts',(-26.6843174133755,24.3010917591116,-69.2294842090159));
#9115=CARTESIAN_POINT('Ctrl Pts',(-26.6852093652762,24.2973576339207,-69.2292455677689));
#9116=CARTESIAN_POINT('Ctrl Pts',(-26.6855982132651,24.2957240866685,-69.2291412652521));
#9117=CARTESIAN_POINT('Ctrl Pts',(-26.6864992267176,24.2919257609363,-69.2288989603356));
#9118=CARTESIAN_POINT('Ctrl Pts',(-26.6870104268223,24.2897607591288,-69.2287610146917));
#9119=CARTESIAN_POINT('Ctrl Pts',(-26.6880582266442,24.2853025503532,-69.228477291748));
#9120=CARTESIAN_POINT('Ctrl Pts',(-26.688594555266,24.2830092801167,-69.2283315302066));
#9121=CARTESIAN_POINT('Ctrl Pts',(-26.6899610312855,24.2771373889373,-69.2279587742636));
#9122=CARTESIAN_POINT('Ctrl Pts',(-26.6907875773205,24.2735579205878,-69.2277319861788));
#9123=CARTESIAN_POINT('Ctrl Pts',(-26.6931594201572,24.263205623926,-69.227077340584));
#9124=CARTESIAN_POINT('Ctrl Pts',(-26.6946889527264,24.2564291508383,-69.2266503708514));
#9125=CARTESIAN_POINT('Ctrl Pts',(-26.6997851973655,24.2335057722964,-69.2252111030123));
#9126=CARTESIAN_POINT('Ctrl Pts',(-26.7032496120129,24.2173360651036,-69.2242043809806));
#9127=CARTESIAN_POINT('Ctrl Pts',(-26.7505442485847,23.987991038212,-69.2100365037298));
#9128=CARTESIAN_POINT('Ctrl Pts',(-26.7728001214968,23.770912029779,-69.197959250513));
#9129=CARTESIAN_POINT('Ctrl Pts',(-26.7730011573562,23.5532288202234,-69.185795593234));
#9130=CARTESIAN_POINT('Ctrl Pts',(-26.7730011574137,23.5532287579762,-69.1857955897558));
#9131=CARTESIAN_POINT('Ctrl Pts',(-26.7732054564558,23.3320075218539,-69.173434235357));
#9132=CARTESIAN_POINT('Ctrl Pts',(-26.7506327281678,23.1113721182886,-69.1610278023702));
#9133=CARTESIAN_POINT('Ctrl Pts',(-26.6957738384993,22.8472819083673,-69.1449756089575));
#9134=CARTESIAN_POINT('Ctrl Pts',(-26.6848338097548,22.8000046968289,-69.1420561916178));
#9135=CARTESIAN_POINT('Ctrl Pts',(-26.6711261504128,22.7463166407036,-69.1386825548652));
#9136=CARTESIAN_POINT('Ctrl Pts',(-26.6693997950522,22.739644482657,-69.1382622576606));
#9137=CARTESIAN_POINT('Ctrl Pts',(-26.6665470351507,22.7287629593386,-69.1375750931814));
#9138=CARTESIAN_POINT('Ctrl Pts',(-26.6654334659043,22.7245502266217,-69.1373086419016));
#9139=CARTESIAN_POINT('Ctrl Pts',(-26.6632566903651,22.7163823715248,-69.1367912148915));
#9140=CARTESIAN_POINT('Ctrl Pts',(-26.6621944812802,22.7124269901385,-69.1365402719437));
#9141=CARTESIAN_POINT('Ctrl Pts',(-26.6603350152416,22.7055551602477,-69.136103647351));
#9142=CARTESIAN_POINT('Ctrl Pts',(-26.6595411867571,22.7026377824156,-69.1359180774591));
#9143=CARTESIAN_POINT('Ctrl Pts',(-26.6578788088884,22.6965621823505,-69.1355311897376));
#9144=CARTESIAN_POINT('Ctrl Pts',(-26.657009548073,22.6934041598527,-69.1353298489175));
#9145=CARTESIAN_POINT('Ctrl Pts',(-26.6546079598432,22.6847308946379,-69.1347762155896));
#9146=CARTESIAN_POINT('Ctrl Pts',(-26.653065755952,22.6792184203156,-69.1344236014498));
#9147=CARTESIAN_POINT('Ctrl Pts',(-26.6470575178138,22.6579609360606,-69.1330609500813));
#9148=CARTESIAN_POINT('Ctrl Pts',(-26.6424863169952,22.6422461358809,-69.1320474841022));
#9149=CARTESIAN_POINT('Ctrl Pts',(-26.5643782701371,22.3811594630158,-69.1151058043699));
#9150=CARTESIAN_POINT('Ctrl Pts',(-26.4619812884204,22.1454344618131,-69.0981648042478));
#9151=CARTESIAN_POINT('Ctrl Pts',(-26.3100444919523,21.8854098902804,-69.0778085857863));
#9152=CARTESIAN_POINT('Ctrl Pts',(-26.2864698453787,21.8469417935336,-69.0747534967972));
#9153=CARTESIAN_POINT('Ctrl Pts',(-26.2387812909853,21.7726719841405,-69.0687801124473));
#9154=CARTESIAN_POINT('Ctrl Pts',(-26.21473993205,21.7368340865593,-69.0658622234479));
#9155=CARTESIAN_POINT('Ctrl Pts',(-26.125634952176,21.609606645508,-69.055395730578));
#9156=CARTESIAN_POINT('Ctrl Pts',(-26.0565246181369,21.5211380394106,-69.0479103490364));
#9157=CARTESIAN_POINT('Ctrl Pts',(-25.9531289354647,21.4021446022513,-69.0377241156348));
#9158=CARTESIAN_POINT('Ctrl Pts',(-25.9225982140616,21.3684736284577,-69.0348277388908));
#9159=CARTESIAN_POINT('Ctrl Pts',(-25.8889201513319,21.3328748081639,-69.0317608990171));
#9160=CARTESIAN_POINT('Ctrl Pts',(-25.8864724042136,21.3302960205248,-69.0315387098154));
#9161=CARTESIAN_POINT('Ctrl Pts',(-25.8824304113453,21.3260517279102,-69.031172984435));
#9162=CARTESIAN_POINT('Ctrl Pts',(-25.8808386450638,21.3243838819002,-69.0310292591087));
#9163=CARTESIAN_POINT('Ctrl Pts',(-25.8777320295428,21.321135769037,-69.0307493403345));
#9164=CARTESIAN_POINT('Ctrl Pts',(-25.8762173577638,21.3195553352059,-69.0306131332645));
#9165=CARTESIAN_POINT('Ctrl Pts',(-25.8735391891196,21.3167665828567,-69.0303727788705));
#9166=CARTESIAN_POINT('Ctrl Pts',(-25.8723763650497,21.3155576355581,-69.0302685799365));
#9167=CARTESIAN_POINT('Ctrl Pts',(-25.8698920198838,21.3129787821633,-69.0300463018101));
#9168=CARTESIAN_POINT('Ctrl Pts',(-25.8685702327196,21.3116091427938,-69.0299282444383));
#9169=CARTESIAN_POINT('Ctrl Pts',(-25.8647550876547,21.3076628820449,-69.0295880766785));
#9170=CARTESIAN_POINT('Ctrl Pts',(-25.862258632085,21.3050892391217,-69.029366208838));
#9171=CARTESIAN_POINT('Ctrl Pts',(-25.8512192622192,21.2937464834782,-69.0283882592297));
#9172=CARTESIAN_POINT('Ctrl Pts',(-25.8426305687554,21.285021773659,-69.0276357235385));
#9173=CARTESIAN_POINT('Ctrl Pts',(-25.6864115514974,21.1281272087986,-69.0140926395539));
#9174=CARTESIAN_POINT('Ctrl Pts',(-25.5247255038059,20.9946014998495,-69.0023806990977));
#9175=CARTESIAN_POINT('Ctrl Pts',(-25.29662468742,20.8408919410459,-68.9870047288095));
#9176=CARTESIAN_POINT('Ctrl Pts',(-25.2409229168375,20.8057882684458,-68.9833322874066));
#9177=CARTESIAN_POINT('Ctrl Pts',(-25.1284920881933,20.7396560833252,-68.9760170442883));
#9178=CARTESIAN_POINT('Ctrl Pts',(-25.0718272940134,20.7085800743964,-68.972376638843));
#9179=CARTESIAN_POINT('Ctrl Pts',(-24.9123068813412,20.6272361352512,-68.9621843669601));
#9180=CARTESIAN_POINT('Ctrl Pts',(-24.807657461768,20.5807162187292,-68.9555574778011));
#9181=CARTESIAN_POINT('Ctrl Pts',(-24.6697707422643,20.5280187026143,-68.9467673547709));
#9182=CARTESIAN_POINT('Ctrl Pts',(-24.6385988385386,20.5166539202363,-68.9447767753158));
#9183=CARTESIAN_POINT('Ctrl Pts',(-24.587795553332,20.4990156545212,-68.9415243201679));
#9184=CARTESIAN_POINT('Ctrl Pts',(-24.568269251572,20.4924454858257,-68.9402722900324));
#9185=CARTESIAN_POINT('Ctrl Pts',(-24.5444434316439,20.4846821302062,-68.9387418084519));
#9186=CARTESIAN_POINT('Ctrl Pts',(-24.5402023756834,20.4833099599962,-68.9384692729771));
#9187=CARTESIAN_POINT('Ctrl Pts',(-24.5319904220197,20.4806718359171,-68.9379413520671));
#9188=CARTESIAN_POINT('Ctrl Pts',(-24.5280198864919,20.4794047769494,-68.9376860035972));
#9189=CARTESIAN_POINT('Ctrl Pts',(-24.5211563656972,20.4772291828694,-68.9372444364809));
#9190=CARTESIAN_POINT('Ctrl Pts',(-24.5182645285773,20.4763170198311,-68.9370583375375));
#9191=CARTESIAN_POINT('Ctrl Pts',(-24.5122775444319,20.4744378506011,-68.9366729475509));
#9192=CARTESIAN_POINT('Ctrl Pts',(-24.5091822176633,20.473471432102,-68.9364736374142));
#9193=CARTESIAN_POINT('Ctrl Pts',(-24.5007761467483,20.4708608178706,-68.9359321995467));
#9194=CARTESIAN_POINT('Ctrl Pts',(-24.4954626161897,20.4692256954772,-68.9355897742052));
#9195=CARTESIAN_POINT('Ctrl Pts',(-24.4755631049716,20.4631583800688,-68.9343066810395));
#9196=CARTESIAN_POINT('Ctrl Pts',(-24.4609501457871,20.4588160046311,-68.9333630741039));
#9197=CARTESIAN_POINT('Ctrl Pts',(-24.2105540254591,20.386337920182,-68.9171689827774));
#9198=CARTESIAN_POINT('Ctrl Pts',(-23.9678294973073,20.3452665866028,-68.900994467619));
#9199=CARTESIAN_POINT('Ctrl Pts',(-23.566312469373,20.3237321235846,-68.8738500861061));
#9200=CARTESIAN_POINT('Ctrl Pts',(-23.4093689591525,20.3267690235554,-68.8631694872695));
#9201=CARTESIAN_POINT('Ctrl Pts',(-23.1549473069267,20.3503148935474,-68.8462090337969));
#9202=CARTESIAN_POINT('Ctrl Pts',(-23.0570858717645,20.3639289059037,-68.8397756024135));
#9203=CARTESIAN_POINT('Ctrl Pts',(-22.9532715709775,20.3832700476603,-68.8331530916662));
#9204=CARTESIAN_POINT('Ctrl Pts',(-22.9465531061393,20.3845438705476,-68.8327254277066));
#9205=CARTESIAN_POINT('Ctrl Pts',(-22.9377584459771,20.3862403563334,-68.8321668545844));
#9206=CARTESIAN_POINT('Ctrl Pts',(-22.935678607299,20.3866436838143,-68.8320348500308));
#9207=CARTESIAN_POINT('Ctrl Pts',(-22.9315799292667,20.387442704064,-68.8317748953788));
#9208=CARTESIAN_POINT('Ctrl Pts',(-22.9295610684081,20.3878382795429,-68.8316469386188));
#9209=CARTESIAN_POINT('Ctrl Pts',(-22.9256935726164,20.388599922605,-68.8314019836878));
#9210=CARTESIAN_POINT('Ctrl Pts',(-22.9238448857191,20.3889656774206,-68.8312849682221));
#9211=CARTESIAN_POINT('Ctrl Pts',(-22.9196050641498,20.3898083731706,-68.831016771518));
#9212=CARTESIAN_POINT('Ctrl Pts',(-22.9172141437238,20.3902864073637,-68.830865653456));
#9213=CARTESIAN_POINT('Ctrl Pts',(-22.9096687311686,20.3918039241972,-68.8303891290036));
#9214=CARTESIAN_POINT('Ctrl Pts',(-22.9045162056152,20.392853315598,-68.8300642900469));
#9215=CARTESIAN_POINT('Ctrl Pts',(-22.8619302032348,20.401635218107,-68.8273839705886));
#9216=CARTESIAN_POINT('Ctrl Pts',(-22.8246324541351,20.4100209424876,-68.8250652452798));
#9217=CARTESIAN_POINT('Ctrl Pts',(-22.6264503396226,20.4582984475591,-68.8128558338109));
#9218=CARTESIAN_POINT('Ctrl Pts',(-22.468655968898,20.5098985066632,-68.8035203906868));
#9219=CARTESIAN_POINT('Ctrl Pts',(-22.1690608476923,20.6341649479403,-68.785368005679));
#9220=CARTESIAN_POINT('Ctrl Pts',(-22.0272895418607,20.7056367829793,-68.7765676565949));
#9221=CARTESIAN_POINT('Ctrl Pts',(-21.8023962496162,20.8406615327062,-68.7615727199061));
#9222=CARTESIAN_POINT('Ctrl Pts',(-21.7160719219068,20.898335589781,-68.755540453925));
#9223=CARTESIAN_POINT('Ctrl Pts',(-21.6074411569875,20.9787572428591,-68.7474815141315));
#9224=CARTESIAN_POINT('Ctrl Pts',(-21.5824727918744,20.997813139757,-68.7455953601906));
#9225=CARTESIAN_POINT('Ctrl Pts',(-21.5422671963951,21.0294386989259,-68.7425001217097));
#9226=CARTESIAN_POINT('Ctrl Pts',(-21.5268596300861,21.0417891325277,-68.7412997244604));
#9227=CARTESIAN_POINT('Ctrl Pts',(-21.5081582683963,21.0570642212532,-68.7398248084924));
#9228=CARTESIAN_POINT('Ctrl Pts',(-21.5047554599435,21.0598552419691,-68.7395557075462));
#9229=CARTESIAN_POINT('Ctrl Pts',(-21.4981728135297,21.0652769935985,-68.7390337113095));
#9230=CARTESIAN_POINT('Ctrl Pts',(-21.4949922892913,21.0679068808265,-68.7387808506076));
#9231=CARTESIAN_POINT('Ctrl Pts',(-21.4894876407385,21.0724763532925,-68.7383420849296));
#9232=CARTESIAN_POINT('Ctrl Pts',(-21.4871611760068,21.0744131217086,-68.7381562951631));
#9233=CARTESIAN_POINT('Ctrl Pts',(-21.4823344593196,21.0784428625924,-68.7377701044611));
#9234=CARTESIAN_POINT('Ctrl Pts',(-21.479834648984,21.0805363566772,-68.7375696822722));
#9235=CARTESIAN_POINT('Ctrl Pts',(-21.4737552272873,21.0856433533145,-68.7370812633407));
#9236=CARTESIAN_POINT('Ctrl Pts',(-21.4701790010589,21.0886608587815,-68.7367931022605));
#9237=CARTESIAN_POINT('Ctrl Pts',(-21.4567004610959,21.1000839659831,-68.7357038241347));
#9238=CARTESIAN_POINT('Ctrl Pts',(-21.4468425272232,21.1085415295775,-68.7349005646103));
#9239=CARTESIAN_POINT('Ctrl Pts',(-21.2848928897728,21.2491939434784,-68.7215940869746));
#9240=CARTESIAN_POINT('Ctrl Pts',(-21.1455078637019,21.3952814394197,-68.7084827251768));
#9241=CARTESIAN_POINT('Ctrl Pts',(-20.9344557323106,21.6626364538485,-68.6856744553058));
#9242=CARTESIAN_POINT('Ctrl Pts',(-20.8553894982721,21.7773457337308,-68.6762098595937));
#9243=CARTESIAN_POINT('Ctrl Pts',(-20.6997948022966,22.0376594262543,-68.6557485569511));
#9244=CARTESIAN_POINT('Ctrl Pts',(-20.6264702153756,22.1847638390257,-68.6448089919531));
#9245=CARTESIAN_POINT('Ctrl Pts',(-20.5623425906333,22.3425481778775,-68.6341357379712));
#9246=CARTESIAN_POINT('Ctrl Pts',(-20.5600361577521,22.3482701438751,-68.6337500894727));
#9247=CARTESIAN_POINT('Ctrl Pts',(-20.5567583789032,22.3564697201795,-68.6331995099653));
#9248=CARTESIAN_POINT('Ctrl Pts',(-20.5557736671606,22.3589419198697,-68.633033775177));
#9249=CARTESIAN_POINT('Ctrl Pts',(-20.5540856692534,22.3631950936009,-68.6327491070246));
#9250=CARTESIAN_POINT('Ctrl Pts',(-20.5533809073319,22.3649754771267,-68.6326300836762));
#9251=CARTESIAN_POINT('Ctrl Pts',(-20.5520337772088,22.3683875065671,-68.6324022482081));
#9252=CARTESIAN_POINT('Ctrl Pts',(-20.5513911549291,22.3700190461712,-68.632293420522));
#9253=CARTESIAN_POINT('Ctrl Pts',(-20.5498808810348,22.3738626446177,-68.6320373168004));
#9254=CARTESIAN_POINT('Ctrl Pts',(-20.5490143421539,22.3760751438068,-68.6318901085708));
#9255=CARTESIAN_POINT('Ctrl Pts',(-20.546463444579,22.382609521938,-68.6314559687205));
#9256=CARTESIAN_POINT('Ctrl Pts',(-20.544785959525,22.386934104816,-68.6311694511217));
#9257=CARTESIAN_POINT('Ctrl Pts',(-20.5303105558753,22.4244922211805,-68.628687958453));
#9258=CARTESIAN_POINT('Ctrl Pts',(-20.5180543377325,22.4579338126701,-68.6265249641485));
#9259=CARTESIAN_POINT('Ctrl Pts',(-20.4598465109826,22.6252920670263,-68.6158979464249));
#9260=CARTESIAN_POINT('Ctrl Pts',(-20.4221950968812,22.7619461145281,-68.6078411699737));
#9261=CARTESIAN_POINT('Ctrl Pts',(-20.351355410499,23.1061746118789,-68.5880913564939));
#9262=CARTESIAN_POINT('Ctrl Pts',(-20.329234423668,23.3153319300588,-68.5765370200261));
#9263=CARTESIAN_POINT('Ctrl Pts',(-20.3272670541395,23.5679376182818,-68.561972758975));
#9264=CARTESIAN_POINT('Ctrl Pts',(-20.3277858848855,23.6107227685876,-68.5594865754545));
#9265=CARTESIAN_POINT('Ctrl Pts',(-20.3317549958391,23.7345699195833,-68.5522183979401));
#9266=CARTESIAN_POINT('Ctrl Pts',(-20.3374143615516,23.8155230570439,-68.5473777719861));
#9267=CARTESIAN_POINT('Ctrl Pts',(-20.3471831677087,23.906008204228,-68.5418365721243));
#9268=CARTESIAN_POINT('Ctrl Pts',(-20.3482904128051,23.9158397782012,-68.5412327766843));
#9269=CARTESIAN_POINT('Ctrl Pts',(-20.3499744658075,23.9301981679349,-68.5403484042372));
#9270=CARTESIAN_POINT('Ctrl Pts',(-20.35051565203,23.9347291708695,-68.5400689534336));
#9271=CARTESIAN_POINT('Ctrl Pts',(-20.3514771385252,23.94263642828,-68.5395806127939));
#9272=CARTESIAN_POINT('Ctrl Pts',(-20.3518931664677,23.9460132030191,-68.5393718583824));
#9273=CARTESIAN_POINT('Ctrl Pts',(-20.3527074703625,23.9525375163742,-68.538968113238));
#9274=CARTESIAN_POINT('Ctrl Pts',(-20.35310504863,23.9556851396105,-68.5387731448036));
#9275=CARTESIAN_POINT('Ctrl Pts',(-20.3540590702268,23.9631494471666,-68.538310356779));
#9276=CARTESIAN_POINT('Ctrl Pts',(-20.3546196105906,23.967465593815,-68.5380424076923));
#9277=CARTESIAN_POINT('Ctrl Pts',(-20.3566220815938,23.9826437590434,-68.5370989066085));
#9278=CARTESIAN_POINT('Ctrl Pts',(-20.3581106509294,23.9934994533959,-68.5364218786832));
#9279=CARTESIAN_POINT('Ctrl Pts',(-20.3787263421843,24.1383511377345,-68.5273579042963));
#9280=CARTESIAN_POINT('Ctrl Pts',(-20.406218496205,24.2710018614856,-68.5187039035601));
#9281=CARTESIAN_POINT('Ctrl Pts',(-20.4895788516676,24.5753818994669,-68.4979914060277));
#9282=CARTESIAN_POINT('Ctrl Pts',(-20.5516950624083,24.7449305587953,-68.4857818347036));
#9283=CARTESIAN_POINT('Ctrl Pts',(-20.7076333505371,25.0804996381276,-68.4607471234247));
#9284=CARTESIAN_POINT('Ctrl Pts',(-20.8026768411822,25.2452414211013,-68.4479752544551));
#9285=CARTESIAN_POINT('Ctrl Pts',(-20.9161667668792,25.4070699014729,-68.4355665400562));
#9286=CARTESIAN_POINT('Ctrl Pts',(-20.9206744529099,25.4134480908651,-68.4350777425127));
#9287=CARTESIAN_POINT('Ctrl Pts',(-20.9268978197079,25.4221863257839,-68.4344085249116));
#9288=CARTESIAN_POINT('Ctrl Pts',(-20.9285935369433,25.424560454571,-68.4342267475036));
#9289=CARTESIAN_POINT('Ctrl Pts',(-20.9314376300577,25.4285309830028,-68.4339228205729));
#9290=CARTESIAN_POINT('Ctrl Pts',(-20.9325842430391,25.4301286340751,-68.4338005490517));
#9291=CARTESIAN_POINT('Ctrl Pts',(-20.9348465129014,25.4332747200059,-68.4335598172978));
#9292=CARTESIAN_POINT('Ctrl Pts',(-20.9359620829553,25.4348232134354,-68.4334413513428));
#9293=CARTESIAN_POINT('Ctrl Pts',(-20.9384261553047,25.4382371291764,-68.4331802182592));
#9294=CARTESIAN_POINT('Ctrl Pts',(-20.9397752842585,25.4401021028061,-68.4330375947565));
#9295=CARTESIAN_POINT('Ctrl Pts',(-20.9445023637839,25.4466218793069,-68.4325390942446));
#9296=CARTESIAN_POINT('Ctrl Pts',(-20.9478908016322,25.4512691195356,-68.4321839426802));
#9297=CARTESIAN_POINT('Ctrl Pts',(-20.9825985447377,25.4986040651552,-68.4285680223459));
#9298=CARTESIAN_POINT('Ctrl Pts',(-21.0149550564518,25.5405259316187,-68.425378177054));
#9299=CARTESIAN_POINT('Ctrl Pts',(-21.0500078055271,25.5836981146262,-68.4220842515412));
#9300=CARTESIAN_POINT('Ctrl Pts',(-21.0516860069556,25.5857598274346,-68.4219269263743));
#9301=CARTESIAN_POINT('Ctrl Pts',(-21.0558601057756,25.5908748731096,-68.4215365465891));
#9302=CARTESIAN_POINT('Ctrl Pts',(-21.0583590660969,25.5939257127944,-68.4213036527697));
#9303=CARTESIAN_POINT('Ctrl Pts',(-21.0632948537146,25.5999290245701,-68.4208452504473));
#9304=CARTESIAN_POINT('Ctrl Pts',(-21.0657313534115,25.6028817559857,-68.4206197257744));
#9305=CARTESIAN_POINT('Ctrl Pts',(-21.0782132507519,25.6179534614436,-68.4194682299248));
#9306=CARTESIAN_POINT('Ctrl Pts',(-21.0883422291366,25.6300032425262,-68.4185464718938));
#9307=CARTESIAN_POINT('Ctrl Pts',(-21.1235507570112,25.6712708426543,-68.4153838205948));
#9308=CARTESIAN_POINT('Ctrl Pts',(-21.1490660277703,25.7001138614991,-68.4131631185877));
#9309=CARTESIAN_POINT('Ctrl Pts',(-21.3197387950159,25.8862158926064,-68.3987146211547));
#9310=CARTESIAN_POINT('Ctrl Pts',(-21.4797387776913,26.029142824665,-68.3870084901483));
#9311=CARTESIAN_POINT('Ctrl Pts',(-21.7177415225729,26.2025137702741,-68.3703281466061));
#9312=CARTESIAN_POINT('Ctrl Pts',(-21.7844974519291,26.2474166211357,-68.3657237322359));
#9313=CARTESIAN_POINT('Ctrl Pts',(-21.9252348712095,26.3346167649304,-68.356080755321));
#9314=CARTESIAN_POINT('Ctrl Pts',(-21.9993515053438,26.3765699462487,-68.3510364005855));
#9315=CARTESIAN_POINT('Ctrl Pts',(-22.0750360157945,26.4155367747871,-68.3458849806668));
#9316=CARTESIAN_POINT('Origin',(-23.5502525316942,23.5502525316942,-77.3107734492734));
#9317=CARTESIAN_POINT('',(-22.0750360151859,26.4155367744738,-66.8490341587423));
#9318=CARTESIAN_POINT('',(-22.0750362583504,26.4155368996692,-67.093261398997));
#9319=CARTESIAN_POINT('',(-22.0750360153461,26.4155367745563,-77.3107734492734));
#9320=CARTESIAN_POINT('Ctrl Pts',(-22.0750360151859,26.4155367744738,-66.8490341587423));
#9321=CARTESIAN_POINT('Ctrl Pts',(-22.071751051794,26.4138454824967,-66.8492740680067));
#9322=CARTESIAN_POINT('Ctrl Pts',(-22.0684689450228,26.4121485146271,-66.8495137316808));
#9323=CARTESIAN_POINT('Ctrl Pts',(-22.0349331677317,26.3947361476878,-66.8519621261606));
#9324=CARTESIAN_POINT('Ctrl Pts',(-22.0049264016203,26.3785465723192,-66.8541492954419));
#9325=CARTESIAN_POINT('Ctrl Pts',(-21.964865452227,26.3561044828296,-66.8570588277654));
#9326=CARTESIAN_POINT('Ctrl Pts',(-21.9545817318059,26.3502689730423,-66.8578047646124));
#9327=CARTESIAN_POINT('Ctrl Pts',(-21.9373738941877,26.3403787722159,-66.8590510549417));
#9328=CARTESIAN_POINT('Ctrl Pts',(-21.9304324762743,26.33635463476,-66.8595532715316));
#9329=CARTESIAN_POINT('Ctrl Pts',(-21.9209876518421,26.3308319721612,-66.8602358228901));
#9330=CARTESIAN_POINT('Ctrl Pts',(-21.9184712210249,26.3293559532637,-66.8604176017749));
#9331=CARTESIAN_POINT('Ctrl Pts',(-21.9144516998785,26.3269909512494,-66.8607078321521));
#9332=CARTESIAN_POINT('Ctrl Pts',(-21.9129473294202,26.3261041643728,-66.8608164270686));
#9333=CARTESIAN_POINT('Ctrl Pts',(-21.9098154495445,26.3242545716661,-66.861042445296));
#9334=CARTESIAN_POINT('Ctrl Pts',(-21.9081880702867,26.32329155826,-66.8611598539729));
#9335=CARTESIAN_POINT('Ctrl Pts',(-21.904428276986,26.3210622032338,-66.861431029932));
#9336=CARTESIAN_POINT('Ctrl Pts',(-21.9022964706173,26.3197948285625,-66.861584729307));
#9337=CARTESIAN_POINT('Ctrl Pts',(-21.8956311006471,26.3158217960736,-66.8620651167713));
#9338=CARTESIAN_POINT('Ctrl Pts',(-21.8911026918383,26.3131074402995,-66.8623912372227));
#9339=CARTESIAN_POINT('Ctrl Pts',(-21.8518358796182,26.2894393181381,-66.8652170937012));
#9340=CARTESIAN_POINT('Ctrl Pts',(-21.8174873797379,26.2678412933784,-66.8676753559295));
#9341=CARTESIAN_POINT('Ctrl Pts',(-21.7782668974541,26.2421337395313,-66.8704774438764));
#9342=CARTESIAN_POINT('Ctrl Pts',(-21.7729899996083,26.2386526913302,-66.8708543459155));
#9343=CARTESIAN_POINT('Ctrl Pts',(-21.7654881496936,26.2336721525225,-66.8713900690177));
#9344=CARTESIAN_POINT('Ctrl Pts',(-21.7632548080461,26.2321853974609,-66.871549544547));
#9345=CARTESIAN_POINT('Ctrl Pts',(-21.7531504520879,26.2254406143342,-66.8722710205149));
#9346=CARTESIAN_POINT('Ctrl Pts',(-21.7453006928116,26.2201506618071,-66.8728313954879));
#9347=CARTESIAN_POINT('Ctrl Pts',(-21.7308608046311,26.210326832863,-66.8738622294787));
#9348=CARTESIAN_POINT('Ctrl Pts',(-21.7242640556973,26.2058028761522,-66.874333160156));
#9349=CARTESIAN_POINT('Ctrl Pts',(-21.5120675976051,26.059117003706,-66.8894839192787));
#9350=CARTESIAN_POINT('Ctrl Pts',(-21.3236662234413,25.8935276903796,-66.9030665896908));
#9351=CARTESIAN_POINT('Ctrl Pts',(-21.1321606329539,25.6810382666368,-66.9192090352863));
#9352=CARTESIAN_POINT('Ctrl Pts',(-21.1084853449075,25.6538658999633,-66.9212510764056));
#9353=CARTESIAN_POINT('Ctrl Pts',(-21.0539628711192,25.5891290779866,-66.9260746124904));
#9354=CARTESIAN_POINT('Ctrl Pts',(-21.0235004978678,25.5512531647835,-66.9288651041417));
#9355=CARTESIAN_POINT('Ctrl Pts',(-20.9520944112749,25.4582375507148,-66.935664541135));
#9356=CARTESIAN_POINT('Ctrl Pts',(-20.912035480991,25.4024518423534,-66.9396993171218));
#9357=CARTESIAN_POINT('Ctrl Pts',(-20.8492623044331,25.3088623054611,-66.94643113152));
#9358=CARTESIAN_POINT('Ctrl Pts',(-20.8254870293839,25.2717952147458,-66.9490880873586));
#9359=CARTESIAN_POINT('Ctrl Pts',(-20.7984718782925,25.2277147876981,-66.9522413434687));
#9360=CARTESIAN_POINT('Ctrl Pts',(-20.7944876405969,25.2211613407394,-66.9527099722501));
#9361=CARTESIAN_POINT('Ctrl Pts',(-20.7884258489683,25.2111099873883,-66.9534285016709));
#9362=CARTESIAN_POINT('Ctrl Pts',(-20.7863314431698,25.2076222338793,-66.9536777843918));
#9363=CARTESIAN_POINT('Ctrl Pts',(-20.7825277638771,25.2012608150456,-66.9541323857964));
#9364=CARTESIAN_POINT('Ctrl Pts',(-20.7808163452368,25.1983884335812,-66.9543376256966));
#9365=CARTESIAN_POINT('Ctrl Pts',(-20.7773875797564,25.1926133008575,-66.9547502237295));
#9366=CARTESIAN_POINT('Ctrl Pts',(-20.7756703135225,25.1897105068309,-66.9549575844667));
#9367=CARTESIAN_POINT('Ctrl Pts',(-20.7708049971634,25.1814568436622,-66.9555471128667));
#9368=CARTESIAN_POINT('Ctrl Pts',(-20.7676678602695,25.1760995878717,-66.955929677077));
#9369=CARTESIAN_POINT('Ctrl Pts',(-20.7544825273087,25.1534331884865,-66.9575479682772));
#9370=CARTESIAN_POINT('Ctrl Pts',(-20.7445803801854,25.136039996924,-66.9587889732221));
#9371=CARTESIAN_POINT('Ctrl Pts',(-20.5471565920339,24.7816256852889,-66.9840643800981));
#9372=CARTESIAN_POINT('Ctrl Pts',(-20.4215136068534,24.4137811638311,-67.0106387641172));
#9373=CARTESIAN_POINT('Ctrl Pts',(-20.3516565360621,23.9523693850203,-67.041736694716));
#9374=CARTESIAN_POINT('Ctrl Pts',(-20.3425375520877,23.8716263032723,-67.0470763542266));
#9375=CARTESIAN_POINT('Ctrl Pts',(-20.3348873412828,23.7693405300435,-67.0536452722395));
#9376=CARTESIAN_POINT('Ctrl Pts',(-20.3335072014444,23.7480463505507,-67.0550021280944));
#9377=CARTESIAN_POINT('Ctrl Pts',(-20.3318795093429,23.7183683735257,-67.0568768781347));
#9378=CARTESIAN_POINT('Ctrl Pts',(-20.3314530598292,23.7099954840798,-67.0574039839134));
#9379=CARTESIAN_POINT('Ctrl Pts',(-20.3308614440077,23.697413427129,-67.0581932617872));
#9380=CARTESIAN_POINT('Ctrl Pts',(-20.3306718529067,23.6932055235595,-67.0584567531634));
#9381=CARTESIAN_POINT('Ctrl Pts',(-20.330344477475,23.6856083254168,-67.0589316088834));
#9382=CARTESIAN_POINT('Ctrl Pts',(-20.3302037937746,23.6822191721242,-67.0591431332316));
#9383=CARTESIAN_POINT('Ctrl Pts',(-20.3299844317609,23.6767253071739,-67.0594855053579));
#9384=CARTESIAN_POINT('Ctrl Pts',(-20.3299024657812,23.6746207407398,-67.0596165380963));
#9385=CARTESIAN_POINT('Ctrl Pts',(-20.3297517455885,23.6706507611359,-67.0598634820847));
#9386=CARTESIAN_POINT('Ctrl Pts',(-20.3296825494338,23.6687853809422,-67.0599794173715));
#9387=CARTESIAN_POINT('Ctrl Pts',(-20.3295309201338,23.6645996097572,-67.0602393513081));
#9388=CARTESIAN_POINT('Ctrl Pts',(-20.3294493740323,23.6622791942414,-67.0603832990458));
#9389=CARTESIAN_POINT('Ctrl Pts',(-20.3292486230738,23.6563853115175,-67.0607485548853));
#9390=CARTESIAN_POINT('Ctrl Pts',(-20.3291328568721,23.652811719765,-67.0609696692688));
#9391=CARTESIAN_POINT('Ctrl Pts',(-20.3285292586741,23.6331691412746,-67.0621831667186));
#9392=CARTESIAN_POINT('Ctrl Pts',(-20.3281557110311,23.6170964964791,-67.0631692092188));
#9393=CARTESIAN_POINT('Ctrl Pts',(-20.3278091554453,23.5951002452893,-67.0645100272));
#9394=CARTESIAN_POINT('Ctrl Pts',(-20.3277321868415,23.5891788562458,-67.0648701194979));
#9395=CARTESIAN_POINT('Ctrl Pts',(-20.3242828337794,23.2523838765508,-67.085304367825));
#9396=CARTESIAN_POINT('Ctrl Pts',(-20.3718685107923,22.9229043021577,-67.1028787001028));
#9397=CARTESIAN_POINT('Ctrl Pts',(-20.4977740286207,22.5118546766074,-67.1273582830588));
#9398=CARTESIAN_POINT('Ctrl Pts',(-20.5310674179644,22.4186987619381,-67.1330730897336));
#9399=CARTESIAN_POINT('Ctrl Pts',(-20.5763410767344,22.3083243574325,-67.1401313089737));
#9400=CARTESIAN_POINT('Ctrl Pts',(-20.5842734977606,22.2894974901052,-67.1413454995848));
#9401=CARTESIAN_POINT('Ctrl Pts',(-20.6101175801385,22.2297529822681,-67.1452327994348));
#9402=CARTESIAN_POINT('Ctrl Pts',(-20.6287005104431,22.1891331115147,-67.147927394233));
#9403=CARTESIAN_POINT('Ctrl Pts',(-20.6514687183023,22.1419808096554,-67.1511209150155));
#9404=CARTESIAN_POINT('Ctrl Pts',(-20.654841340632,22.1350596568794,-67.1515913453299));
#9405=CARTESIAN_POINT('Ctrl Pts',(-20.6600367049817,22.1244942633115,-67.1523120660817));
#9406=CARTESIAN_POINT('Ctrl Pts',(-20.6618416272569,22.1208412501776,-67.1525617327008));
#9407=CARTESIAN_POINT('Ctrl Pts',(-20.6651403993394,22.1141965690248,-67.1530167366055));
#9408=CARTESIAN_POINT('Ctrl Pts',(-20.6666319889595,22.1112037800658,-67.1532219943883));
#9409=CARTESIAN_POINT('Ctrl Pts',(-20.6696356736158,22.1052004810458,-67.1536343753121));
#9410=CARTESIAN_POINT('Ctrl Pts',(-20.671147836676,22.1021900098686,-67.1538415006528));
#9411=CARTESIAN_POINT('Ctrl Pts',(-20.6754515241984,22.0936554570164,-67.1544296290452));
#9412=CARTESIAN_POINT('Ctrl Pts',(-20.6782542345898,22.0881370604565,-67.1548110256027));
#9413=CARTESIAN_POINT('Ctrl Pts',(-20.6901171594478,22.0649452733546,-67.1564186270837));
#9414=CARTESIAN_POINT('Ctrl Pts',(-20.6993245944035,22.0473480546261,-67.1576500240077));
#9415=CARTESIAN_POINT('Ctrl Pts',(-20.8898527224905,21.6912631792552,-67.1828086426594));
#9416=CARTESIAN_POINT('Ctrl Pts',(-21.130048976372,21.3878442960755,-67.2092502191314));
#9417=CARTESIAN_POINT('Ctrl Pts',(-21.5015603771647,21.0599791741555,-67.2422889545621));
#9418=CARTESIAN_POINT('Ctrl Pts',(-21.589131135369,20.9904459012406,-67.2496037491309));
#9419=CARTESIAN_POINT('Ctrl Pts',(-21.6839723599596,20.9228701956236,-67.2569071892691));
#9420=CARTESIAN_POINT('Ctrl Pts',(-21.6878032162492,20.9201532622064,-67.25720117977));
#9421=CARTESIAN_POINT('Ctrl Pts',(-21.6939118655706,20.9158409034196,-67.2576683471058));
#9422=CARTESIAN_POINT('Ctrl Pts',(-21.696185789952,20.9142400481883,-67.2578418907974));
#9423=CARTESIAN_POINT('Ctrl Pts',(-21.7004400201947,20.9112532749489,-67.2581658969187));
#9424=CARTESIAN_POINT('Ctrl Pts',(-21.7024198161109,20.9098666394216,-67.2583164084264));
#9425=CARTESIAN_POINT('Ctrl Pts',(-21.7059340486127,20.9074111833929,-67.2585830894818));
#9426=CARTESIAN_POINT('Ctrl Pts',(-21.7074678578092,20.9063414694437,-67.2586993208817));
#9427=CARTESIAN_POINT('Ctrl Pts',(-21.7104478408215,20.9042670134367,-67.2589248246702));
#9428=CARTESIAN_POINT('Ctrl Pts',(-21.7118939045229,20.9032621234517,-67.2590341074075));
#9429=CARTESIAN_POINT('Ctrl Pts',(-21.7153171301786,20.9008874341177,-67.2592924682951));
#9430=CARTESIAN_POINT('Ctrl Pts',(-21.7172950068385,20.8995186596967,-67.2594414756641));
#9431=CARTESIAN_POINT('Ctrl Pts',(-21.7231855766921,20.8954518814136,-67.2598844604298));
#9432=CARTESIAN_POINT('Ctrl Pts',(-21.72710272977,20.8927603019372,-67.2601779996104));
#9433=CARTESIAN_POINT('Ctrl Pts',(-21.7630097728024,20.8682043810405,-67.262859398056));
#9434=CARTESIAN_POINT('Ctrl Pts',(-21.7953873245048,20.8469087884076,-67.2652093414131));
#9435=CARTESIAN_POINT('Ctrl Pts',(-21.9259093773667,20.7643944499013,-67.2744486117063));
#9436=CARTESIAN_POINT('Ctrl Pts',(-22.0269425287747,20.7078894589182,-67.2810849149984));
#9437=CARTESIAN_POINT('Ctrl Pts',(-22.262067571359,20.592538203951,-67.2958828648194));
#9438=CARTESIAN_POINT('Ctrl Pts',(-22.3975620943591,20.5371477059052,-67.3039721913078));
#9439=CARTESIAN_POINT('Ctrl Pts',(-22.7267607808419,20.4280389775623,-67.3234757196262));
#9440=CARTESIAN_POINT('Ctrl Pts',(-22.9226162703508,20.3828543723098,-67.3349856079639));
#9441=CARTESIAN_POINT('Ctrl Pts',(-23.1382557662779,20.3539005451125,-67.3481725507862));
#9442=CARTESIAN_POINT('Ctrl Pts',(-23.1551451316106,20.3517689094322,-67.3492084622403));
#9443=CARTESIAN_POINT('Ctrl Pts',(-23.1776167155095,20.3491134331594,-67.350591095949));
#9444=CARTESIAN_POINT('Ctrl Pts',(-23.1831847660175,20.3484701789342,-67.3509340406014));
#9445=CARTESIAN_POINT('Ctrl Pts',(-23.1923445467277,20.3474361944824,-67.351498795709));
#9446=CARTESIAN_POINT('Ctrl Pts',(-23.1959353220984,20.3470369706635,-67.3517203375232));
#9447=CARTESIAN_POINT('Ctrl Pts',(-23.2029052318732,20.3462739164794,-67.3521506557007));
#9448=CARTESIAN_POINT('Ctrl Pts',(-23.2062842867353,20.3459093915537,-67.3523594098266));
#9449=CARTESIAN_POINT('Ctrl Pts',(-23.2141024765704,20.345078491738,-67.3528427196324));
#9450=CARTESIAN_POINT('Ctrl Pts',(-23.2185420087843,20.3446159935571,-67.3531173973127));
#9451=CARTESIAN_POINT('Ctrl Pts',(-23.2304808782954,20.3433973020056,-67.3538566959056));
#9452=CARTESIAN_POINT('Ctrl Pts',(-23.2379818973771,20.3426581957637,-67.3543218550933));
#9453=CARTESIAN_POINT('Ctrl Pts',(-23.273342085281,20.3392992207581,-67.3565178455768));
#9454=CARTESIAN_POINT('Ctrl Pts',(-23.3012313257525,20.3370160138398,-67.3582592536592));
#9455=CARTESIAN_POINT('Ctrl Pts',(-23.3370482099445,20.3345528848333,-67.3605083291293));
#9456=CARTESIAN_POINT('Ctrl Pts',(-23.3449522690451,20.3340385926062,-67.3610054434393));
#9457=CARTESIAN_POINT('Ctrl Pts',(-23.3570955233167,20.3332934153709,-67.3617704001531));
#9458=CARTESIAN_POINT('Ctrl Pts',(-23.36133345261,20.3330417572404,-67.3620375947915));
#9459=CARTESIAN_POINT('Ctrl Pts',(-23.3690222317799,20.33260042414,-67.3625227772735));
#9460=CARTESIAN_POINT('Ctrl Pts',(-23.372472918515,20.332407924532,-67.3627406772435));
#9461=CARTESIAN_POINT('Ctrl Pts',(-23.3828768238727,20.3318443195515,-67.3633981121929));
#9462=CARTESIAN_POINT('Ctrl Pts',(-23.3898309085838,20.3314901998071,-67.3638381699023));
#9463=CARTESIAN_POINT('Ctrl Pts',(-23.4030417205749,20.3308603899949,-67.3646753430994));
#9464=CARTESIAN_POINT('Ctrl Pts',(-23.4092982187891,20.3305803953213,-67.3650723247186));
#9465=CARTESIAN_POINT('Ctrl Pts',(-23.4196371531477,20.3301478944543,-67.3657291802957));
#9466=CARTESIAN_POINT('Ctrl Pts',(-23.423719153876,20.3299849099055,-67.365988734928));
#9467=CARTESIAN_POINT('Ctrl Pts',(-23.4334470095938,20.3296150247619,-67.3666077981251));
#9468=CARTESIAN_POINT('Ctrl Pts',(-23.4390931066583,20.3294152084763,-67.3669675197026));
#9469=CARTESIAN_POINT('Ctrl Pts',(-23.4654739110495,20.328551037455,-67.3686502217297));
#9470=CARTESIAN_POINT('Ctrl Pts',(-23.4862138374949,20.3280720670423,-67.3699787234017));
#9471=CARTESIAN_POINT('Ctrl Pts',(-23.5329382121105,20.3274442928584,-67.3729843306236));
#9472=CARTESIAN_POINT('Ctrl Pts',(-23.5589225365494,20.3274094542109,-67.3746646308278));
#9473=CARTESIAN_POINT('Ctrl Pts',(-23.6430720573178,20.3283142912047,-67.3801345173751));
#9474=CARTESIAN_POINT('Ctrl Pts',(-23.7012099266834,20.3305145350434,-67.3839576085634));
#9475=CARTESIAN_POINT('Ctrl Pts',(-23.9980600324472,20.3498064370695,-67.4036846520479));
#9476=CARTESIAN_POINT('Ctrl Pts',(-24.2343727315032,20.3918741136768,-67.4201457873064));
#9477=CARTESIAN_POINT('Ctrl Pts',(-24.4886744942841,20.4670476477931,-67.4377576368294));
#9478=CARTESIAN_POINT('Ctrl Pts',(-24.5134188492056,20.4746877310232,-67.439469361579));
#9479=CARTESIAN_POINT('Ctrl Pts',(-24.6036801529953,20.5037530630241,-67.4457000023894));
#9480=CARTESIAN_POINT('Ctrl Pts',(-24.6686025004669,20.5269821569794,-67.4501559133535));
#9481=CARTESIAN_POINT('Ctrl Pts',(-24.7395454230503,20.5549639682586,-67.4549587808422));
#9482=CARTESIAN_POINT('Ctrl Pts',(-24.7463467231649,20.5576734020386,-67.4554185451053));
#9483=CARTESIAN_POINT('Ctrl Pts',(-24.7566790302439,20.5618303346241,-67.4561158924241));
#9484=CARTESIAN_POINT('Ctrl Pts',(-24.7602167410417,20.5632609453658,-67.4563544606313));
#9485=CARTESIAN_POINT('Ctrl Pts',(-24.7659890453827,20.5656071384672,-67.4567433857277));
#9486=CARTESIAN_POINT('Ctrl Pts',(-24.7682251528049,20.5665189496962,-67.4568939675727));
#9487=CARTESIAN_POINT('Ctrl Pts',(-24.7724173703301,20.568233896433,-67.4571761189404));
#9488=CARTESIAN_POINT('Ctrl Pts',(-24.7743737170115,20.569036444665,-67.45730772392));
#9489=CARTESIAN_POINT('Ctrl Pts',(-24.778024225884,20.5705381849039,-67.4575531746687));
#9490=CARTESIAN_POINT('Ctrl Pts',(-24.7797185789884,20.5712368955936,-67.4576670493902));
#9491=CARTESIAN_POINT('Ctrl Pts',(-24.7831243447033,20.5726447524607,-67.4578958460064));
#9492=CARTESIAN_POINT('Ctrl Pts',(-24.7848357355404,20.5733539262515,-67.4580107656039));
#9493=CARTESIAN_POINT('Ctrl Pts',(-24.7896248236885,20.5753432901539,-67.4583322138294));
#9494=CARTESIAN_POINT('Ctrl Pts',(-24.7927011590756,20.576626784879,-67.4585385405241));
#9495=CARTESIAN_POINT('Ctrl Pts',(-24.8051639181609,20.5818491571695,-67.4593737780938));
#9496=CARTESIAN_POINT('Ctrl Pts',(-24.8145337789328,20.5858277786903,-67.4600002902994));
#9497=CARTESIAN_POINT('Ctrl Pts',(-24.9754185188145,20.6550440577152,-67.4707355176587));
#9498=CARTESIAN_POINT('Ctrl Pts',(-25.1217474526536,20.731786553067,-67.4801642266036));
#9499=CARTESIAN_POINT('Ctrl Pts',(-25.3332568178811,20.8643318796997,-67.4942066115237));
#9500=CARTESIAN_POINT('Ctrl Pts',(-25.4031445689615,20.9120589346875,-67.498920790241));
#9501=CARTESIAN_POINT('Ctrl Pts',(-25.539309842123,21.013130137849,-67.5084025450122));
#9502=CARTESIAN_POINT('Ctrl Pts',(-25.6055139479192,21.0664572755107,-67.5131665683818));
#9503=CARTESIAN_POINT('Ctrl Pts',(-25.760197156275,21.2014771634436,-67.5248274306774));
#9504=CARTESIAN_POINT('Ctrl Pts',(-25.8463503498309,21.2856264148833,-67.5317798649994));
#9505=CARTESIAN_POINT('Ctrl Pts',(-25.9626848560045,21.412733038289,-67.5420326543951));
#9506=CARTESIAN_POINT('Ctrl Pts',(-25.9968439326092,21.4519176334225,-67.545161885981));
#9507=CARTESIAN_POINT('Ctrl Pts',(-26.035153800727,21.498071405352,-67.5488192657515));
#9508=CARTESIAN_POINT('Ctrl Pts',(-26.0402454838774,21.5042523390233,-67.5493084868189));
#9509=CARTESIAN_POINT('Ctrl Pts',(-26.0479342234198,21.5136571210728,-67.5500520304206));
#9510=CARTESIAN_POINT('Ctrl Pts',(-26.0505482185001,21.5168671333914,-67.5503056660621));
#9511=CARTESIAN_POINT('Ctrl Pts',(-26.0552651099531,21.5226823714651,-67.5507648869279));
#9512=CARTESIAN_POINT('Ctrl Pts',(-26.0573701485495,21.5252858586339,-67.5509703852374));
#9513=CARTESIAN_POINT('Ctrl Pts',(-26.0615621424405,21.5304870243109,-67.5513807358947));
#9514=CARTESIAN_POINT('Ctrl Pts',(-26.0636491336283,21.5330846687992,-67.5515855864451));
#9515=CARTESIAN_POINT('Ctrl Pts',(-26.0694871206834,21.5403742437401,-67.5521601861726));
#9516=CARTESIAN_POINT('Ctrl Pts',(-26.0732290181079,21.5450734137672,-67.5525302999729));
#9517=CARTESIAN_POINT('Ctrl Pts',(-26.0883944406577,21.5642281928463,-67.554037777636));
#9518=CARTESIAN_POINT('Ctrl Pts',(-26.0997068643056,21.5787709548677,-67.5551795652177));
#9519=CARTESIAN_POINT('Ctrl Pts',(-26.3524216448012,21.9094627578509,-67.5810854230835));
#9520=CARTESIAN_POINT('Ctrl Pts',(-26.5333078805176,22.2674707544445,-67.6085842138839));
#9521=CARTESIAN_POINT('Ctrl Pts',(-26.6649475526173,22.7194932560586,-67.6398489527027));
#9522=CARTESIAN_POINT('Ctrl Pts',(-26.683031076185,22.7905247362341,-67.6446490201181));
#9523=CARTESIAN_POINT('Ctrl Pts',(-26.7051164100945,22.8915716196957,-67.651263941748));
#9524=CARTESIAN_POINT('Ctrl Pts',(-26.7111409669596,22.9211173337465,-67.6531726554586));
#9525=CARTESIAN_POINT('Ctrl Pts',(-26.717589536486,22.9551775643618,-67.6553404317211));
#9526=CARTESIAN_POINT('Ctrl Pts',(-26.7184195308325,22.9596123833538,-67.6556220544685));
#9527=CARTESIAN_POINT('Ctrl Pts',(-26.7196613443168,22.9663255660196,-67.6560473866775));
#9528=CARTESIAN_POINT('Ctrl Pts',(-26.7200800216135,22.9686026309767,-67.6561914872142));
#9529=CARTESIAN_POINT('Ctrl Pts',(-26.720831743408,22.9727159463238,-67.6564514840381));
#9530=CARTESIAN_POINT('Ctrl Pts',(-26.7211656458436,22.9745520299008,-67.6565674293454));
#9531=CARTESIAN_POINT('Ctrl Pts',(-26.7218318120067,22.9782333480822,-67.6567996752139));
#9532=CARTESIAN_POINT('Ctrl Pts',(-26.7221640590032,22.980078575172,-67.656915974505));
#9533=CARTESIAN_POINT('Ctrl Pts',(-26.7231020964033,22.9853144240414,-67.6572456602924));
#9534=CARTESIAN_POINT('Ctrl Pts',(-26.7237040641018,22.9887057415903,-67.6574588273678));
#9535=CARTESIAN_POINT('Ctrl Pts',(-26.7262142214823,23.0029802126301,-67.6583545248056));
#9536=CARTESIAN_POINT('Ctrl Pts',(-26.7280719018647,23.0138723445563,-67.6590341997011));
#9537=CARTESIAN_POINT('Ctrl Pts',(-26.7584198765389,23.1975050770158,-67.6704325206091));
#9538=CARTESIAN_POINT('Ctrl Pts',(-26.772848032414,23.3723036917934,-67.6803894010009));
#9539=CARTESIAN_POINT('Ctrl Pts',(-26.7732050218955,23.7802177939754,-67.703286709911));
#9540=CARTESIAN_POINT('Ctrl Pts',(-26.7481879453314,24.0123239489652,-67.7161030452746));
#9541=CARTESIAN_POINT('Ctrl Pts',(-26.6781518770707,24.3321171492653,-67.7351934171007));
#9542=CARTESIAN_POINT('Ctrl Pts',(-26.6538566894063,24.4235824524446,-67.7408166252732));
#9543=CARTESIAN_POINT('Ctrl Pts',(-26.6225041918604,24.5236449799105,-67.7471996671686));
#9544=CARTESIAN_POINT('Ctrl Pts',(-26.6193854133437,24.5334343422323,-67.7478266062952));
#9545=CARTESIAN_POINT('Ctrl Pts',(-26.6149489598046,24.5471328563189,-67.7487074204629));
#9546=CARTESIAN_POINT('Ctrl Pts',(-26.6136704855726,24.5510547187893,-67.7489600017864));
#9547=CARTESIAN_POINT('Ctrl Pts',(-26.6113160478814,24.5582304370356,-67.7494228899342));
#9548=CARTESIAN_POINT('Ctrl Pts',(-26.6102424153966,24.5614850565324,-67.7496331195022));
#9549=CARTESIAN_POINT('Ctrl Pts',(-26.6080610625296,24.5680623461763,-67.7500585473707));
#9550=CARTESIAN_POINT('Ctrl Pts',(-26.6069531132843,24.5713849344991,-67.7502737529827));
#9551=CARTESIAN_POINT('Ctrl Pts',(-26.6042212328238,24.5795331830353,-67.750802249253));
#9552=CARTESIAN_POINT('Ctrl Pts',(-26.6025912817329,24.5843568016986,-67.7511157390762));
#9553=CARTESIAN_POINT('Ctrl Pts',(-26.5966572988239,24.6017813548035,-67.7522504624634));
#9554=CARTESIAN_POINT('Ctrl Pts',(-26.592286656865,24.6143593138189,-67.753073904751));
#9555=CARTESIAN_POINT('Ctrl Pts',(-26.5290596319906,24.7927424773087,-67.7648148322503));
#9556=CARTESIAN_POINT('Ctrl Pts',(-26.4568105201193,24.9534542286004,-67.7761899271129));
#9557=CARTESIAN_POINT('Ctrl Pts',(-26.2190176758691,25.3843246831993,-67.8089339146691));
#9558=CARTESIAN_POINT('Ctrl Pts',(-26.0263021806489,25.6371886486296,-67.8309963779814));
#9559=CARTESIAN_POINT('Ctrl Pts',(-25.7881142690445,25.8693819625022,-67.852051117757));
#9560=CARTESIAN_POINT('Ctrl Pts',(-25.7762844832101,25.8807392298604,-67.8530827821655));
#9561=CARTESIAN_POINT('Ctrl Pts',(-25.7617514503933,25.89448013669,-67.8543326170052));
#9562=CARTESIAN_POINT('Ctrl Pts',(-25.7591305127118,25.8969499124231,-67.8545573265785));
#9563=CARTESIAN_POINT('Ctrl Pts',(-25.7548071145975,25.9010102992609,-67.8549268558224));
#9564=CARTESIAN_POINT('Ctrl Pts',(-25.7531070689303,25.9026034576033,-67.8550718720046));
#9565=CARTESIAN_POINT('Ctrl Pts',(-25.7500414104437,25.9054701305853,-67.8553328523499));
#9566=CARTESIAN_POINT('Ctrl Pts',(-25.7486764216167,25.9067442990198,-67.8554488672698));
#9567=CARTESIAN_POINT('Ctrl Pts',(-25.7457418388022,25.9094788585167,-67.8556978855248));
#9568=CARTESIAN_POINT('Ctrl Pts',(-25.7441718990837,25.9109388658469,-67.8558308590629));
#9569=CARTESIAN_POINT('Ctrl Pts',(-25.7398757322299,25.9149262135952,-67.8561940754672));
#9570=CARTESIAN_POINT('Ctrl Pts',(-25.7371465763807,25.917450415236,-67.8564240761353));
#9571=CARTESIAN_POINT('Ctrl Pts',(-25.7230531224797,25.930440304171,-67.8576080677669));
#9572=CARTESIAN_POINT('Ctrl Pts',(-25.71161779156,25.9408291306661,-67.8585562435994));
#9573=CARTESIAN_POINT('Ctrl Pts',(-25.6396851604433,26.0052407462451,-67.8644462974042));
#9574=CARTESIAN_POINT('Ctrl Pts',(-25.5772356739585,26.0570508146548,-67.8692343574641));
#9575=CARTESIAN_POINT('Ctrl Pts',(-25.386876903964,26.2032074151032,-67.8831216776298));
#9576=CARTESIAN_POINT('Ctrl Pts',(-25.2538713563161,26.2905167893736,-67.8919424957213));
#9577=CARTESIAN_POINT('Ctrl Pts',(-24.8966057948266,26.4889317200474,-67.9147877020739));
#9578=CARTESIAN_POINT('Ctrl Pts',(-24.664931977241,26.5843861364605,-67.9288874924147));
#9579=CARTESIAN_POINT('Ctrl Pts',(-24.4094598853148,26.6563959654596,-67.9449843920653));
#9580=CARTESIAN_POINT('Ctrl Pts',(-24.3943101485948,26.6605468961141,-67.9459405519521));
#9581=CARTESIAN_POINT('Ctrl Pts',(-24.373691506772,26.6660345361635,-67.9472442390154));
#9582=CARTESIAN_POINT('Ctrl Pts',(-24.3682483797659,26.667467961682,-67.9475886228678));
#9583=CARTESIAN_POINT('Ctrl Pts',(-24.3596504283398,26.6697081269951,-67.948132971767));
#9584=CARTESIAN_POINT('Ctrl Pts',(-24.3564980707704,26.6705243622792,-67.9483326286105));
#9585=CARTESIAN_POINT('Ctrl Pts',(-24.3501531630389,26.6721569827243,-67.9487346439706));
#9586=CARTESIAN_POINT('Ctrl Pts',(-24.3469605871147,26.6729732517857,-67.9489370059866));
#9587=CARTESIAN_POINT('Ctrl Pts',(-24.3397129197359,26.6748144774001,-67.9493965833787));
#9588=CARTESIAN_POINT('Ctrl Pts',(-24.3356570796745,26.6758364375571,-67.9496538953936));
#9589=CARTESIAN_POINT('Ctrl Pts',(-24.3271787994683,26.6779551866641,-67.9501920527244));
#9590=CARTESIAN_POINT('Ctrl Pts',(-24.3227560026073,26.6790504974548,-67.9504729452809));
#9591=CARTESIAN_POINT('Ctrl Pts',(-24.3111776945373,26.6818918322999,-67.9512087014476));
#9592=CARTESIAN_POINT('Ctrl Pts',(-24.3040185244873,26.683622704401,-67.9516640538967));
#9593=CARTESIAN_POINT('Ctrl Pts',(-24.282791797508,26.6886777311922,-67.9530154213757));
#9594=CARTESIAN_POINT('Ctrl Pts',(-24.2687078816998,26.6919317654591,-67.9539136914976));
#9595=CARTESIAN_POINT('Ctrl Pts',(-24.1172557803307,26.7258525288661,-67.963591615875));
#9596=CARTESIAN_POINT('Ctrl Pts',(-23.9780605426976,26.7475793384602,-67.9726583067093));
#9597=CARTESIAN_POINT('Ctrl Pts',(-23.496658752439,26.7907201907011,-68.0045849088361));
#9598=CARTESIAN_POINT('Ctrl Pts',(-23.1527573792706,26.766690978291,-68.0286145521784));
#9599=CARTESIAN_POINT('Ctrl Pts',(-22.8168138996899,26.6884352691511,-68.0504163696479));
#9600=CARTESIAN_POINT('Ctrl Pts',(-22.8145183953754,26.687897891085,-68.0505652477791));
#9601=CARTESIAN_POINT('Ctrl Pts',(-22.7998120974257,26.6844381173085,-68.0515184345704));
#9602=CARTESIAN_POINT('Ctrl Pts',(-22.7874179093343,26.6814445542802,-68.0523189746117));
#9603=CARTESIAN_POINT('Ctrl Pts',(-22.7715065231558,26.6775013994235,-68.053342811172));
#9604=CARTESIAN_POINT('Ctrl Pts',(-22.7679729428501,26.6766193482592,-68.05356993695));
#9605=CARTESIAN_POINT('Ctrl Pts',(-22.7625839280838,26.6752644355901,-68.0539159389616));
#9606=CARTESIAN_POINT('Ctrl Pts',(-22.7607274224574,26.6747959112192,-68.0540350663526));
#9607=CARTESIAN_POINT('Ctrl Pts',(-22.7572457636202,26.6739139474559,-68.0542583436697));
#9608=CARTESIAN_POINT('Ctrl Pts',(-22.7556205214727,26.6735008956411,-68.0543625155747));
#9609=CARTESIAN_POINT('Ctrl Pts',(-22.7518890041494,26.6725494372758,-68.0546015674004));
#9610=CARTESIAN_POINT('Ctrl Pts',(-22.7497829547693,26.67201016886,-68.0547363962404));
#9611=CARTESIAN_POINT('Ctrl Pts',(-22.7439454141031,26.6705091306908,-68.0551098666797));
#9612=CARTESIAN_POINT('Ctrl Pts',(-22.7402150840443,26.669542794756,-68.0553482425941));
#9613=CARTESIAN_POINT('Ctrl Pts',(-22.7197893057333,26.6642124181877,-68.056651999071));
#9614=CARTESIAN_POINT('Ctrl Pts',(-22.703126967369,26.6597209193522,-68.057710068957));
#9615=CARTESIAN_POINT('Ctrl Pts',(-22.514395727657,26.6072168555052,-68.0696408052974));
#9616=CARTESIAN_POINT('Ctrl Pts',(-22.3465420371194,26.5451031631022,-68.0797511401937));
#9617=CARTESIAN_POINT('Ctrl Pts',(-22.1477807606247,26.4521226584926,-68.0920478323319));
#9618=CARTESIAN_POINT('Ctrl Pts',(-22.1112256544791,26.4341693271435,-68.0943230976292));
#9619=CARTESIAN_POINT('Ctrl Pts',(-22.0750358851076,26.4155367075019,-68.0965974740783));
#9620=CARTESIAN_POINT('Ctrl Pts',(-22.0750360157945,26.4155367747871,-68.3458849806668));
#9621=CARTESIAN_POINT('Ctrl Pts',(-22.0784800904417,26.4173099865772,-68.3456505618322));
#9622=CARTESIAN_POINT('Ctrl Pts',(-22.0819274119822,26.4190770143301,-68.3454159240608));
#9623=CARTESIAN_POINT('Ctrl Pts',(-22.1000493232814,26.4283247196044,-68.3441824765203));
#9624=CARTESIAN_POINT('Ctrl Pts',(-22.1147776462151,26.4356988926478,-68.3431800025512));
#9625=CARTESIAN_POINT('Ctrl Pts',(-22.1345180773245,26.4453939805772,-68.3418361501642));
#9626=CARTESIAN_POINT('Ctrl Pts',(-22.1394807380538,26.4478154732018,-68.3414982920684));
#9627=CARTESIAN_POINT('Ctrl Pts',(-22.1477066037292,26.451803079866,-68.3409382335229));
#9628=CARTESIAN_POINT('Ctrl Pts',(-22.1509662810733,26.4533764788072,-68.340716287486));
#9629=CARTESIAN_POINT('Ctrl Pts',(-22.1572895536721,26.4564155068332,-68.3402857225853));
#9630=CARTESIAN_POINT('Ctrl Pts',(-22.1603528298417,26.4578817919093,-68.3400771269128));
#9631=CARTESIAN_POINT('Ctrl Pts',(-22.167433093088,26.4612571251992,-68.3395949643483));
#9632=CARTESIAN_POINT('Ctrl Pts',(-22.1714517188969,26.4631627022122,-68.339321277289));
#9633=CARTESIAN_POINT('Ctrl Pts',(-22.1843408556698,26.4692419049337,-68.3384433930214));
#9634=CARTESIAN_POINT('Ctrl Pts',(-22.193226406766,26.4733833465295,-68.3378380818868));
#9635=CARTESIAN_POINT('Ctrl Pts',(-22.2739725679157,26.5105705876087,-68.3323361470576));
#9636=CARTESIAN_POINT('Ctrl Pts',(-22.3470024779112,26.5409984354011,-68.3273499512269));
#9637=CARTESIAN_POINT('Ctrl Pts',(-22.6564194201477,26.6567488357286,-68.3061548249634));
#9638=CARTESIAN_POINT('Ctrl Pts',(-22.9012234463537,26.7169508790242,-68.2891287255201));
#9639=CARTESIAN_POINT('Ctrl Pts',(-23.3228565381973,26.7696603634558,-68.2604080780132));
#9640=CARTESIAN_POINT('Ctrl Pts',(-23.4967179673015,26.7772396510975,-68.2487643023647));
#9641=CARTESIAN_POINT('Ctrl Pts',(-23.6808931592916,26.770370797301,-68.2371622998617));
#9642=CARTESIAN_POINT('Ctrl Pts',(-23.6914223141958,26.769926384422,-68.2365016165205));
#9643=CARTESIAN_POINT('Ctrl Pts',(-23.7051855390367,26.7692778224324,-68.2356415612344));
#9644=CARTESIAN_POINT('Ctrl Pts',(-23.7084215905964,26.7691204395468,-68.2354395997703));
#9645=CARTESIAN_POINT('Ctrl Pts',(-23.7137068327937,26.7688554063312,-68.2351101751449));
#9646=CARTESIAN_POINT('Ctrl Pts',(-23.7157561575824,26.7687506788188,-68.2349825472355));
#9647=CARTESIAN_POINT('Ctrl Pts',(-23.7196890228894,26.7685459297002,-68.2347378190075));
#9648=CARTESIAN_POINT('Ctrl Pts',(-23.7215725700187,26.7684462121119,-68.2346207021154));
#9649=CARTESIAN_POINT('Ctrl Pts',(-23.7259017343548,26.7682132087198,-68.2343517235821));
#9650=CARTESIAN_POINT('Ctrl Pts',(-23.7283472938307,26.7680787882024,-68.2341999263548));
#9651=CARTESIAN_POINT('Ctrl Pts',(-23.7361008319568,26.7676437476764,-68.2337191277751));
#9652=CARTESIAN_POINT('Ctrl Pts',(-23.7414082563328,26.7673327789503,-68.2333907084708));
#9653=CARTESIAN_POINT('Ctrl Pts',(-23.7863714986409,26.7645866626437,-68.2306141261715));
#9654=CARTESIAN_POINT('Ctrl Pts',(-23.8259821122112,26.7614313842311,-68.2282057061306));
#9655=CARTESIAN_POINT('Ctrl Pts',(-23.8728775071728,26.7568216091346,-68.2253883366565));
#9656=CARTESIAN_POINT('Ctrl Pts',(-23.8802261584932,26.7560737261433,-68.2249478383477));
#9657=CARTESIAN_POINT('Ctrl Pts',(-23.8890469371909,26.7551453711082,-68.2244202191382));
#9658=CARTESIAN_POINT('Ctrl Pts',(-23.8905215303371,26.7549891464438,-68.2243320533106));
#9659=CARTESIAN_POINT('Ctrl Pts',(-23.9024548386151,26.7537165518442,-68.2236188628334));
#9660=CARTESIAN_POINT('Ctrl Pts',(-23.9129082593774,26.7525499916206,-68.2229959902271));
#9661=CARTESIAN_POINT('Ctrl Pts',(-23.9283451153248,26.750750741518,-68.2220787008993));
#9662=CARTESIAN_POINT('Ctrl Pts',(-23.9333329860731,26.7501575551131,-68.2217827012626));
#9663=CARTESIAN_POINT('Ctrl Pts',(-23.9709267436019,26.7455975282852,-68.2195545453931));
#9664=CARTESIAN_POINT('Ctrl Pts',(-24.0034726606456,26.7411439569627,-68.2176414698609));
#9665=CARTESIAN_POINT('Ctrl Pts',(-24.3250060409816,26.6921265413384,-68.1988499944521));
#9666=CARTESIAN_POINT('Ctrl Pts',(-24.6067325817623,26.6089269571759,-68.1831276867525));
#9667=CARTESIAN_POINT('Ctrl Pts',(-24.9734276884765,26.4438189216082,-68.1599211303569));
#9668=CARTESIAN_POINT('Ctrl Pts',(-25.0710904728618,26.3937014967322,-68.1534605827957));
#9669=CARTESIAN_POINT('Ctrl Pts',(-25.18225261423,26.3292894300583,-68.1456822957136));
#9670=CARTESIAN_POINT('Ctrl Pts',(-25.198421245754,26.319730861378,-68.1445401007965));
#9671=CARTESIAN_POINT('Ctrl Pts',(-25.2194747788549,26.3070347738638,-68.1430382390958));
#9672=CARTESIAN_POINT('Ctrl Pts',(-25.2244362908768,26.3040244868406,-68.1426832387379));
#9673=CARTESIAN_POINT('Ctrl Pts',(-25.2325335867233,26.2990816610022,-68.1421021091637));
#9674=CARTESIAN_POINT('Ctrl Pts',(-25.2356742510349,26.297157109221,-68.1418762741044));
#9675=CARTESIAN_POINT('Ctrl Pts',(-25.2416854406524,26.2934593524039,-68.141443191835));
#9676=CARTESIAN_POINT('Ctrl Pts',(-25.2445564958741,26.2916870145009,-68.1412359768192));
#9677=CARTESIAN_POINT('Ctrl Pts',(-25.2510842204731,26.2876431979735,-68.1407640074133));
#9678=CARTESIAN_POINT('Ctrl Pts',(-25.2547391270093,26.2853688984127,-68.1404991489235));
#9679=CARTESIAN_POINT('Ctrl Pts',(-25.2660644041576,26.2782901228092,-68.1396765725892));
#9680=CARTESIAN_POINT('Ctrl Pts',(-25.2737190501793,26.2734606833423,-68.1391179296153));
#9681=CARTESIAN_POINT('Ctrl Pts',(-25.3316843564147,26.236547148918,-68.1348670737323));
#9682=CARTESIAN_POINT('Ctrl Pts',(-25.3811126830478,26.2031054210016,-68.1311242991763));
#9683=CARTESIAN_POINT('Ctrl Pts',(-25.6985041993822,25.9752714099105,-68.1062808534322));
#9684=CARTESIAN_POINT('Ctrl Pts',(-25.9360447515623,25.7419650368599,-68.0835106180908));
#9685=CARTESIAN_POINT('Ctrl Pts',(-26.2058460910446,25.3801296670172,-68.0533429093268));
#9686=CARTESIAN_POINT('Ctrl Pts',(-26.2723901226845,25.2795882198733,-68.0454351638608));
#9687=CARTESIAN_POINT('Ctrl Pts',(-26.3363334801124,25.170101365381,-68.0374888059718));
#9688=CARTESIAN_POINT('Ctrl Pts',(-26.3394964476948,25.1646489123233,-68.0370947555206));
#9689=CARTESIAN_POINT('Ctrl Pts',(-26.3439687554558,25.1568869863472,-68.0365362194115));
#9690=CARTESIAN_POINT('Ctrl Pts',(-26.3452912447253,25.1545851663327,-68.0363708856159));
#9691=CARTESIAN_POINT('Ctrl Pts',(-26.3475621455862,25.1506212855754,-68.036086692442));
#9692=CARTESIAN_POINT('Ctrl Pts',(-26.3485119222728,25.1489600119676,-68.0359677438524));
#9693=CARTESIAN_POINT('Ctrl Pts',(-26.3503298791325,25.1457736035065,-68.0357398976184));
#9694=CARTESIAN_POINT('Ctrl Pts',(-26.3511982918493,25.1442486078939,-68.0356309846625));
#9695=CARTESIAN_POINT('Ctrl Pts',(-26.3532422838618,25.1406523819512,-68.0353744586498));
#9696=CARTESIAN_POINT('Ctrl Pts',(-26.3544168156778,25.1385805529072,-68.0352269139529));
#9697=CARTESIAN_POINT('Ctrl Pts',(-26.3578825924931,25.1324512288149,-68.0347911282637));
#9698=CARTESIAN_POINT('Ctrl Pts',(-26.3601673479413,25.1283900420373,-68.0345033057377));
#9699=CARTESIAN_POINT('Ctrl Pts',(-26.3801109719946,25.0927593347981,-68.0319860424262));
#9700=CARTESIAN_POINT('Ctrl Pts',(-26.3972468705161,25.0608979347183,-68.029789605925));
#9701=CARTESIAN_POINT('Ctrl Pts',(-26.5523131082429,24.7605623935644,-68.0095265364863));
#9702=CARTESIAN_POINT('Ctrl Pts',(-26.6524414014193,24.4742113244679,-67.9933497485836));
#9703=CARTESIAN_POINT('Ctrl Pts',(-26.7323108665828,24.072076712465,-67.9700912053233));
#9704=CARTESIAN_POINT('Ctrl Pts',(-26.7480167369792,23.9650980305409,-67.9638691624895));
#9705=CARTESIAN_POINT('Ctrl Pts',(-26.7647437242686,23.7904683663333,-67.95350672074));
#9706=CARTESIAN_POINT('Ctrl Pts',(-26.7690627938796,23.723217138511,-67.9494678271452));
#9707=CARTESIAN_POINT('Ctrl Pts',(-26.7715497343834,23.6473825387869,-67.9448431257346));
#9708=CARTESIAN_POINT('Ctrl Pts',(-26.7717948598616,23.6388805857829,-67.9443236565793));
#9709=CARTESIAN_POINT('Ctrl Pts',(-26.7721118002692,23.6261367453701,-67.9435434989027));
#9710=CARTESIAN_POINT('Ctrl Pts',(-26.7722089014323,23.6218954770629,-67.9432836047076));
#9711=CARTESIAN_POINT('Ctrl Pts',(-26.7723612634414,23.6146120016928,-67.9428368573164));
#9712=CARTESIAN_POINT('Ctrl Pts',(-26.7724205911742,23.6115698778603,-67.9426501320736));
#9713=CARTESIAN_POINT('Ctrl Pts',(-26.7725337133575,23.6053149836192,-67.9422659379238));
#9714=CARTESIAN_POINT('Ctrl Pts',(-26.7725870112654,23.6021022082078,-67.9420684536102));
#9715=CARTESIAN_POINT('Ctrl Pts',(-26.7727035004709,23.5943843371599,-67.9415936946047));
#9716=CARTESIAN_POINT('Ctrl Pts',(-26.7727620491826,23.5898791868663,-67.9413162743871));
#9717=CARTESIAN_POINT('Ctrl Pts',(-26.772940640945,23.5734925341815,-67.9403061474606));
#9718=CARTESIAN_POINT('Ctrl Pts',(-26.7730044201929,23.5616106268333,-67.9395716764783));
#9719=CARTESIAN_POINT('Ctrl Pts',(-26.7729724555403,23.3649313425468,-67.9273797248113));
#9720=CARTESIAN_POINT('Ctrl Pts',(-26.7570482654972,23.1805131479998,-67.9154146073358));
#9721=CARTESIAN_POINT('Ctrl Pts',(-26.6724960515322,22.6939394884019,-67.88249156417));
#9722=CARTESIAN_POINT('Ctrl Pts',(-26.5760327321624,22.3985878083025,-67.8609585946284));
#9723=CARTESIAN_POINT('Ctrl Pts',(-26.431766003029,22.1069012557221,-67.8403630474853));
#9724=CARTESIAN_POINT('Ctrl Pts',(-26.4244352069993,22.0923578966375,-67.8393385293104));
#9725=CARTESIAN_POINT('Ctrl Pts',(-26.4153530307913,22.0746748150265,-67.8380963028427));
#9726=CARTESIAN_POINT('Ctrl Pts',(-26.4137064133397,22.0714819829437,-67.8378721471503));
#9727=CARTESIAN_POINT('Ctrl Pts',(-26.4109843098647,22.0662253514631,-67.8375033380698));
#9728=CARTESIAN_POINT('Ctrl Pts',(-26.4099119269796,22.0641599634715,-67.8373584894936));
#9729=CARTESIAN_POINT('Ctrl Pts',(-26.4079751125296,22.060439556932,-67.8370976838086));
#9730=CARTESIAN_POINT('Ctrl Pts',(-26.4071114818975,22.058784131932,-67.8369816762687));
#9731=CARTESIAN_POINT('Ctrl Pts',(-26.4052521303924,22.0552276290854,-67.836732533029));
#9732=CARTESIAN_POINT('Ctrl Pts',(-26.4042559519176,22.0533268002683,-67.8365994273819));
#9733=CARTESIAN_POINT('Ctrl Pts',(-26.4015246290244,22.0481277437843,-67.8362355040214));
#9734=CARTESIAN_POINT('Ctrl Pts',(-26.3997856541154,22.0448315154915,-67.836004930075));
#9735=CARTESIAN_POINT('Ctrl Pts',(-26.3907544838809,22.0277846411699,-67.8348132529836));
#9736=CARTESIAN_POINT('Ctrl Pts',(-26.3833682984153,22.0140836303522,-67.8338580553604));
#9737=CARTESIAN_POINT('Ctrl Pts',(-26.3428082480562,21.9401344009479,-67.8287136258538));
#9738=CARTESIAN_POINT('Ctrl Pts',(-26.3078088799976,21.880901652121,-67.8246330857041));
#9739=CARTESIAN_POINT('Ctrl Pts',(-26.2272503068992,21.7540221538762,-67.8158801878081));
#9740=CARTESIAN_POINT('Ctrl Pts',(-26.1809657664963,21.686892668817,-67.8112408980541));
#9741=CARTESIAN_POINT('Ctrl Pts',(-25.9338895648346,21.3561283728473,-67.7879681945281));
#9742=CARTESIAN_POINT('Ctrl Pts',(-25.695873410596,21.1228657480223,-67.7699206021056));
#9743=CARTESIAN_POINT('Ctrl Pts',(-25.4083276543581,20.9169707138947,-67.7485570882266));
#9744=CARTESIAN_POINT('Ctrl Pts',(-25.3900359432607,20.9041585702133,-67.7472009858479));
#9745=CARTESIAN_POINT('Ctrl Pts',(-25.3662677687759,20.8878761120852,-67.7454420269248));
#9746=CARTESIAN_POINT('Ctrl Pts',(-25.3609116357219,20.8842305608477,-67.745045852273));
#9747=CARTESIAN_POINT('Ctrl Pts',(-25.3523899799521,20.8784679815824,-67.7444158446686));
#9748=CARTESIAN_POINT('Ctrl Pts',(-25.3492316156388,20.876340356629,-67.7441824134903));
#9749=CARTESIAN_POINT('Ctrl Pts',(-25.3433143835967,20.8723694560562,-67.7437451998622));
#9750=CARTESIAN_POINT('Ctrl Pts',(-25.3405564234429,20.8705248316107,-67.7435414687391));
#9751=CARTESIAN_POINT('Ctrl Pts',(-25.3343460849178,20.8663849971854,-67.7430828185093));
#9752=CARTESIAN_POINT('Ctrl Pts',(-25.330892121227,20.8640921862613,-67.7428278094452));
#9753=CARTESIAN_POINT('Ctrl Pts',(-25.3207299329009,20.8573745333545,-67.7420777415618));
#9754=CARTESIAN_POINT('Ctrl Pts',(-25.3140096071705,20.8529681345723,-67.7415819910714));
#9755=CARTESIAN_POINT('Ctrl Pts',(-25.2639358181646,20.8204027909067,-67.7378900332445));
#9756=CARTESIAN_POINT('Ctrl Pts',(-25.2199290336381,20.7932668787175,-67.7346559114194));
#9757=CARTESIAN_POINT('Ctrl Pts',(-25.0720873538491,20.7069413214544,-67.7238164528791));
#9758=CARTESIAN_POINT('Ctrl Pts',(-24.965623608188,20.6524742558125,-67.7160471172952));
#9759=CARTESIAN_POINT('Ctrl Pts',(-24.5602369249156,20.4727543754862,-67.6866481181042));
#9760=CARTESIAN_POINT('Ctrl Pts',(-24.2460061689139,20.3868719699905,-67.6640112847241));
#9761=CARTESIAN_POINT('Ctrl Pts',(-23.9205661935998,20.3488467147471,-67.6431997757606));
#9762=CARTESIAN_POINT('Ctrl Pts',(-23.9168689506292,20.348421209674,-67.6429637054893));
#9763=CARTESIAN_POINT('Ctrl Pts',(-23.8976629752918,20.3462445521866,-67.6417393166993));
#9764=CARTESIAN_POINT('Ctrl Pts',(-23.8821420563685,20.344599631626,-67.6407563498027));
#9765=CARTESIAN_POINT('Ctrl Pts',(-23.8620262347386,20.3426154059132,-67.6394913228578));
#9766=CARTESIAN_POINT('Ctrl Pts',(-23.857442037681,20.3421731404327,-67.6392036365385));
#9767=CARTESIAN_POINT('Ctrl Pts',(-23.8504997194681,20.3415183896475,-67.6387688894562));
#9768=CARTESIAN_POINT('Ctrl Pts',(-23.8481423107699,20.3412986760408,-67.6386214235823));
#9769=CARTESIAN_POINT('Ctrl Pts',(-23.8440406582373,20.3409209554131,-67.6383651314467));
#9770=CARTESIAN_POINT('Ctrl Pts',(-23.8422965279682,20.3407617723856,-67.6382562384827));
#9771=CARTESIAN_POINT('Ctrl Pts',(-23.8386433609161,20.3404313581955,-67.6380283447823));
#9772=CARTESIAN_POINT('Ctrl Pts',(-23.8367343020654,20.3402604084193,-67.6379093605524));
#9773=CARTESIAN_POINT('Ctrl Pts',(-23.8322179210524,20.3398600428479,-67.6376281243656));
#9774=CARTESIAN_POINT('Ctrl Pts',(-23.8296104621964,20.3396320994384,-67.637465956101));
#9775=CARTESIAN_POINT('Ctrl Pts',(-23.8208947780506,20.3388808744318,-67.6369245488817));
#9776=CARTESIAN_POINT('Ctrl Pts',(-23.8147852894696,20.3383718414899,-67.6365461117739));
#9777=CARTESIAN_POINT('Ctrl Pts',(-23.8002712315641,20.3372042467812,-67.6356495520246));
#9778=CARTESIAN_POINT('Ctrl Pts',(-23.7918654087687,20.3365612190829,-67.6351322810191));
#9779=CARTESIAN_POINT('Ctrl Pts',(-23.4893182597477,20.3146107686271,-67.6165821986766));
#9780=CARTESIAN_POINT('Ctrl Pts',(-23.1935848608708,20.3337409499986,-67.6006669207868));
#9781=CARTESIAN_POINT('Ctrl Pts',(-22.7062875388641,20.4333969679613,-67.5726752017353));
#9782=CARTESIAN_POINT('Ctrl Pts',(-22.5123262064374,20.492515493757,-67.5610422136581));
#9783=CARTESIAN_POINT('Ctrl Pts',(-22.3135573905142,20.5742046137529,-67.5479834331375));
#9784=CARTESIAN_POINT('Ctrl Pts',(-22.3019403161464,20.5790587164807,-67.5472160717762));
#9785=CARTESIAN_POINT('Ctrl Pts',(-22.2861013960118,20.5857861721426,-67.5461640681359));
#9786=CARTESIAN_POINT('Ctrl Pts',(-22.2818545838601,20.5876007572986,-67.5458814302069));
#9787=CARTESIAN_POINT('Ctrl Pts',(-22.2746314761734,20.5907054366342,-67.5453997352248));
#9788=CARTESIAN_POINT('Ctrl Pts',(-22.271653192098,20.5919909114457,-67.5452008362138));
#9789=CARTESIAN_POINT('Ctrl Pts',(-22.2658949725214,20.5944865708474,-67.5448157344249));
#9790=CARTESIAN_POINT('Ctrl Pts',(-22.2631147934568,20.5956961863503,-67.5446295513194));
#9791=CARTESIAN_POINT('Ctrl Pts',(-22.2565194612862,20.5985767953232,-67.5441872824828));
#9792=CARTESIAN_POINT('Ctrl Pts',(-22.2527058394233,20.6002512619884,-67.5439310778709));
#9793=CARTESIAN_POINT('Ctrl Pts',(-22.2414586774558,20.6052156404535,-67.5431740785274));
#9794=CARTESIAN_POINT('Ctrl Pts',(-22.2340343680099,20.6085262719434,-67.5426725725559));
#9795=CARTESIAN_POINT('Ctrl Pts',(-22.1772312105312,20.6341138944913,-67.5388215791154));
#9796=CARTESIAN_POINT('Ctrl Pts',(-22.1284111481715,20.6576034685148,-67.5354303922328));
#9797=CARTESIAN_POINT('Ctrl Pts',(-21.9655303438327,20.7410926039189,-67.5238280683185));
#9798=CARTESIAN_POINT('Ctrl Pts',(-21.8544946713792,20.8066923947994,-67.5154239235716));
#9799=CARTESIAN_POINT('Ctrl Pts',(-21.5467146396444,21.0143629943626,-67.4907232530375));
#9800=CARTESIAN_POINT('Ctrl Pts',(-21.3616936751148,21.1722068188466,-67.4740247324406));
#9801=CARTESIAN_POINT('Ctrl Pts',(-21.1370673056003,21.4124656417287,-67.4523018067626));
#9802=CARTESIAN_POINT('Ctrl Pts',(-21.0805687684105,21.4779926534535,-67.4466948514009));
#9803=CARTESIAN_POINT('Ctrl Pts',(-21.0228159398043,21.5506970211882,-67.4408744017903));
#9804=CARTESIAN_POINT('Ctrl Pts',(-21.0188770221142,21.555685912914,-67.440476962787));
#9805=CARTESIAN_POINT('Ctrl Pts',(-21.0134290174882,21.5626282933148,-67.4399266446035));
#9806=CARTESIAN_POINT('Ctrl Pts',(-21.0119074094616,21.5645718686067,-67.4397728760596));
#9807=CARTESIAN_POINT('Ctrl Pts',(-21.0092938988829,21.5679180623408,-67.4395086515489));
#9808=CARTESIAN_POINT('Ctrl Pts',(-21.0082009240872,21.5693198356284,-67.4393981185718));
#9809=CARTESIAN_POINT('Ctrl Pts',(-21.0059436617677,21.5722197875276,-67.4391697720245));
#9810=CARTESIAN_POINT('Ctrl Pts',(-21.0047795396782,21.5737180873919,-67.4390519707571));
#9811=CARTESIAN_POINT('Ctrl Pts',(-21.002077877186,21.5772016459136,-67.4387784911596));
#9812=CARTESIAN_POINT('Ctrl Pts',(-21.0005413286407,21.5791876801776,-67.438622884126));
#9813=CARTESIAN_POINT('Ctrl Pts',(-20.9956101654458,21.585576768818,-67.4381232773985));
#9814=CARTESIAN_POINT('Ctrl Pts',(-20.9922245991069,21.5899868431047,-67.4377799203959));
#9815=CARTESIAN_POINT('Ctrl Pts',(-20.9843252167714,21.6003319755168,-67.4369779149572));
#9816=CARTESIAN_POINT('Ctrl Pts',(-20.9798205305044,21.6062740105482,-67.4365198967684));
#9817=CARTESIAN_POINT('Ctrl Pts',(-20.9325757480855,21.6690449299231,-67.431708537571));
#9818=CARTESIAN_POINT('Ctrl Pts',(-20.8917032761629,21.7272628456203,-67.4274792581145));
#9819=CARTESIAN_POINT('Ctrl Pts',(-20.7463138654006,21.9496565464433,-67.4119816426558));
#9820=CARTESIAN_POINT('Ctrl Pts',(-20.6548005518103,22.1218442828833,-67.4012533462879));
#9821=CARTESIAN_POINT('Ctrl Pts',(-20.4900276155911,22.5137725959933,-67.3774436502248));
#9822=CARTESIAN_POINT('Ctrl Pts',(-20.4237548263139,22.7352334912072,-67.3643312298726));
#9823=CARTESIAN_POINT('Ctrl Pts',(-20.3790195206746,22.9761359468739,-67.3494608389825));
#9824=CARTESIAN_POINT('Ctrl Pts',(-20.3764634650916,22.9904386223948,-67.3485760215916));
#9825=CARTESIAN_POINT('Ctrl Pts',(-20.3730818253398,23.0101288761372,-67.3473550828118));
#9826=CARTESIAN_POINT('Ctrl Pts',(-20.3721730355804,23.0155021446788,-67.3470216125165));
#9827=CARTESIAN_POINT('Ctrl Pts',(-20.3707487905723,23.0240549473731,-67.3464903495333));
#9828=CARTESIAN_POINT('Ctrl Pts',(-20.370224462968,23.0272330105053,-67.3462928393996));
#9829=CARTESIAN_POINT('Ctrl Pts',(-20.3692145899599,23.0334117288786,-67.3459086431043));
#9830=CARTESIAN_POINT('Ctrl Pts',(-20.368728523456,23.0364122966847,-67.3457219737242));
#9831=CARTESIAN_POINT('Ctrl Pts',(-20.3675775344247,23.0435817842597,-67.3452757275852));
#9832=CARTESIAN_POINT('Ctrl Pts',(-20.3669165581984,23.0477513236105,-67.345016025713));
#9833=CARTESIAN_POINT('Ctrl Pts',(-20.364964341459,23.0602246468661,-67.3442385743345));
#9834=CARTESIAN_POINT('Ctrl Pts',(-20.3636973930665,23.0685321469252,-67.3437200542545));
#9835=CARTESIAN_POINT('Ctrl Pts',(-20.3532573399508,23.1388323664442,-67.3393259684584));
#9836=CARTESIAN_POINT('Ctrl Pts',(-20.3458623071218,23.2010717693076,-67.3353943454099));
#9837=CARTESIAN_POINT('Ctrl Pts',(-20.3317768545752,23.358738287029,-67.3253200568328));
#9838=CARTESIAN_POINT('Ctrl Pts',(-20.3275119781658,23.4543159449296,-67.3191063655647));
#9839=CARTESIAN_POINT('Ctrl Pts',(-20.3274812262668,23.7661090666804,-67.2985136376937));
#9840=CARTESIAN_POINT('Ctrl Pts',(-20.3492114590003,23.9817287369676,-67.2837255805823));
#9841=CARTESIAN_POINT('Ctrl Pts',(-20.4075866607376,24.2683001928947,-67.2640922445584));
#9842=CARTESIAN_POINT('Ctrl Pts',(-20.4254711337805,24.3425175424531,-67.2590152556615));
#9843=CARTESIAN_POINT('Ctrl Pts',(-20.4499336198544,24.4302283029197,-67.2530740826799));
#9844=CARTESIAN_POINT('Ctrl Pts',(-20.4539897844793,24.4443955449898,-67.2521163278671));
#9845=CARTESIAN_POINT('Ctrl Pts',(-20.4584434809282,24.4595574818779,-67.2510936950582));
#9846=CARTESIAN_POINT('Ctrl Pts',(-20.4587444205512,24.4605801087623,-67.2510247331369));
#9847=CARTESIAN_POINT('Ctrl Pts',(-20.4598796893785,24.4644308251162,-67.2507651000937));
#9848=CARTESIAN_POINT('Ctrl Pts',(-20.4607173949955,24.4672579274898,-67.2505745733691));
#9849=CARTESIAN_POINT('Ctrl Pts',(-20.4620317087834,24.4716712501025,-67.2502772906579));
#9850=CARTESIAN_POINT('Ctrl Pts',(-20.4625056597182,24.4732582523257,-67.2501704188354));
#9851=CARTESIAN_POINT('Ctrl Pts',(-20.4637647093861,24.4774622978841,-67.2498873886278));
#9852=CARTESIAN_POINT('Ctrl Pts',(-20.4645519149317,24.4800787152306,-67.249711323339));
#9853=CARTESIAN_POINT('Ctrl Pts',(-20.4766938118817,24.5202492310955,-67.2470094188855));
#9854=CARTESIAN_POINT('Ctrl Pts',(-20.4887306640684,24.557596068969,-67.2445144727868));
#9855=CARTESIAN_POINT('Ctrl Pts',(-20.5029930314779,24.5992281518378,-67.2417597158957));
#9856=CARTESIAN_POINT('Ctrl Pts',(-20.5045489007792,24.6037370862277,-67.241461714977));
#9857=CARTESIAN_POINT('Ctrl Pts',(-20.5069058677466,24.6105187493381,-67.2410140535087));
#9858=CARTESIAN_POINT('Ctrl Pts',(-20.507699504782,24.6127940357109,-67.2408639533456));
#9859=CARTESIAN_POINT('Ctrl Pts',(-20.5090779171421,24.6167316132686,-67.2406043555559));
#9860=CARTESIAN_POINT('Ctrl Pts',(-20.5096615037599,24.6183943146574,-67.240494786963));
#9861=CARTESIAN_POINT('Ctrl Pts',(-20.5108797626747,24.6218561772695,-67.2402667637747));
#9862=CARTESIAN_POINT('Ctrl Pts',(-20.5115146681793,24.6236552516118,-67.2401483238742));
#9863=CARTESIAN_POINT('Ctrl Pts',(-20.5127814154034,24.6272345875969,-67.239912800371));
#9864=CARTESIAN_POINT('Ctrl Pts',(-20.5134132263574,24.6290148617016,-67.2397957147644));
#9865=CARTESIAN_POINT('Ctrl Pts',(-20.5155889250968,24.6351283390905,-67.2393938377594));
#9866=CARTESIAN_POINT('Ctrl Pts',(-20.5171405343001,24.6394588182017,-67.2391095068396));
#9867=CARTESIAN_POINT('Ctrl Pts',(-20.5299441892682,24.6749537855123,-67.2367816393382));
#9868=CARTESIAN_POINT('Ctrl Pts',(-20.5416674876997,24.7059478360198,-67.2347658146481));
#9869=CARTESIAN_POINT('Ctrl Pts',(-20.5853844978037,24.816350287395,-67.2276273370274));
#9870=CARTESIAN_POINT('Ctrl Pts',(-20.6200633509712,24.8946631223495,-67.2226420781215));
#9871=CARTESIAN_POINT('Ctrl Pts',(-20.7224673267849,25.1030678141482,-67.209352287892));
#9872=CARTESIAN_POINT('Ctrl Pts',(-20.7960152118884,25.2300695081362,-67.2012221498421));
#9873=CARTESIAN_POINT('Ctrl Pts',(-20.9492551310031,25.4573972048921,-67.1858836133517));
#9874=CARTESIAN_POINT('Ctrl Pts',(-21.0267669136445,25.5588355234877,-67.1787068237312));
#9875=CARTESIAN_POINT('Ctrl Pts',(-21.186853587769,25.744398397129,-67.1645497882724));
#9876=CARTESIAN_POINT('Ctrl Pts',(-21.2684278439646,25.8291123010345,-67.1576097116778));
#9877=CARTESIAN_POINT('Ctrl Pts',(-21.3622113556713,25.9164110477373,-67.1498133925124));
#9878=CARTESIAN_POINT('Ctrl Pts',(-21.3700191669768,25.9236072843914,-67.149165656741));
#9879=CARTESIAN_POINT('Ctrl Pts',(-21.3810342056437,25.9336593068333,-67.1482536562228));
#9880=CARTESIAN_POINT('Ctrl Pts',(-21.3842118546138,25.9365475232648,-67.1479907692776));
#9881=CARTESIAN_POINT('Ctrl Pts',(-21.3897361276291,25.9415484984581,-67.1475341043721));
#9882=CARTESIAN_POINT('Ctrl Pts',(-21.3920801077105,25.9436641806056,-67.1473404503256));
#9883=CARTESIAN_POINT('Ctrl Pts',(-21.3969636858578,25.9480591030036,-67.146937210183));
#9884=CARTESIAN_POINT('Ctrl Pts',(-21.3995038008015,25.9503377600644,-67.1467275999003));
#9885=CARTESIAN_POINT('Ctrl Pts',(-21.4054935856725,25.9556938626975,-67.1462336223557));
#9886=CARTESIAN_POINT('Ctrl Pts',(-21.4089462608603,25.9587679224631,-67.1459491133352));
#9887=CARTESIAN_POINT('Ctrl Pts',(-21.4202562563183,25.9687941376048,-67.1450178925139));
#9888=CARTESIAN_POINT('Ctrl Pts',(-21.42814085088,25.9757153004477,-67.1443698862664));
#9889=CARTESIAN_POINT('Ctrl Pts',(-21.4466447157441,25.9917988523318,-67.1428517927588));
#9890=CARTESIAN_POINT('Ctrl Pts',(-21.4572902201461,26.0009306075651,-67.1419804491104));
#9891=CARTESIAN_POINT('Ctrl Pts',(-21.4942860978958,26.0322489388862,-67.1389590701081));
#9892=CARTESIAN_POINT('Ctrl Pts',(-21.5209316187593,26.0540817243844,-67.1367946954634));
#9893=CARTESIAN_POINT('Ctrl Pts',(-21.6431555301754,26.1509967653548,-67.1269160036735));
#9894=CARTESIAN_POINT('Ctrl Pts',(-21.7425745621809,26.2210546553216,-67.1190091605272));
#9895=CARTESIAN_POINT('Ctrl Pts',(-21.9203700980134,26.3318602657314,-67.1051092180637));
#9896=CARTESIAN_POINT('Ctrl Pts',(-21.9968806582552,26.3752978175026,-67.0991996102356));
#9897=CARTESIAN_POINT('Ctrl Pts',(-22.0750362583504,26.4155368996692,-67.093261398997));
#9898=CARTESIAN_POINT('Origin',(-23.5502525316942,23.5502525316942,-77.3107734492734));
#9899=CARTESIAN_POINT('',(-22.0750359980476,26.41553676565,-65.5942565421953));
#9900=CARTESIAN_POINT('',(-22.0750360187516,26.4155367763096,-65.8398919625532));
#9901=CARTESIAN_POINT('',(-22.0750360153461,26.4155367745563,-77.3107734492734));
#9902=CARTESIAN_POINT('',(-26.7730026852622,23.5520333435677,-66.4414554149513));
#9903=CARTESIAN_POINT('Ctrl Pts',(-22.0750359980476,26.41553676565,-65.5942565421953));
#9904=CARTESIAN_POINT('Ctrl Pts',(-22.0582209726656,26.4068794034368,-65.5955036844597));
#9905=CARTESIAN_POINT('Ctrl Pts',(-22.0414809647859,26.3980734084878,-65.5967547895065));
#9906=CARTESIAN_POINT('Ctrl Pts',(-21.7587436008458,26.2461475428026,-65.6180454325648));
#9907=CARTESIAN_POINT('Ctrl Pts',(-21.5141120649862,26.0664943349157,-65.6390626962724));
#9908=CARTESIAN_POINT('Ctrl Pts',(-21.2701080519116,25.8280996323232,-65.6610241028595));
#9909=CARTESIAN_POINT('Ctrl Pts',(-21.2426395348813,25.8002678345547,-65.6635103461838));
#9910=CARTESIAN_POINT('Ctrl Pts',(-21.2120810939885,25.7681567648208,-65.666285134475));
#9911=CARTESIAN_POINT('Ctrl Pts',(-21.2084885232806,25.764363231103,-65.6666114914255));
#9912=CARTESIAN_POINT('Ctrl Pts',(-21.2032117580814,25.7587640815493,-65.6670910308153));
#9913=CARTESIAN_POINT('Ctrl Pts',(-21.2015204111308,25.7569652644205,-65.6672447646115));
#9914=CARTESIAN_POINT('Ctrl Pts',(-21.1985385975009,25.7537866710393,-65.6675158416826));
#9915=CARTESIAN_POINT('Ctrl Pts',(-21.197247275747,25.7524077026796,-65.6676332515294));
#9916=CARTESIAN_POINT('Ctrl Pts',(-21.1945903197741,25.7495654044041,-65.6678748589556));
#9917=CARTESIAN_POINT('Ctrl Pts',(-21.1932248390091,25.7481019407083,-65.6679990446844));
#9918=CARTESIAN_POINT('Ctrl Pts',(-21.1897070267681,25.7443246517358,-65.6683190248789));
#9919=CARTESIAN_POINT('Ctrl Pts',(-21.1875567270587,25.7420089241184,-65.6685146619978));
#9920=CARTESIAN_POINT('Ctrl Pts',(-21.1828832046859,25.7369609858585,-65.6689399751534));
#9921=CARTESIAN_POINT('Ctrl Pts',(-21.1803612943494,25.7342275584416,-65.6691695512294));
#9922=CARTESIAN_POINT('Ctrl Pts',(-21.1730617245074,25.7262882289616,-65.6698342750738));
#9923=CARTESIAN_POINT('Ctrl Pts',(-21.1682964099864,25.7210709317426,-65.6702685014859));
#9924=CARTESIAN_POINT('Ctrl Pts',(-21.0559203874699,25.5972206633023,-65.6805163302563));
#9925=CARTESIAN_POINT('Ctrl Pts',(-20.9572680900283,25.4707260156077,-65.689688718354));
#9926=CARTESIAN_POINT('Ctrl Pts',(-20.7262480933336,25.1240528382958,-65.7131492052165));
#9927=CARTESIAN_POINT('Ctrl Pts',(-20.6100488272049,24.8945168092446,-65.7271874896071));
#9928=CARTESIAN_POINT('Ctrl Pts',(-20.5148784801808,24.6333446197269,-65.7434505356548));
#9929=CARTESIAN_POINT('Ctrl Pts',(-20.5076876810741,24.6129769566681,-65.7447199638977));
#9930=CARTESIAN_POINT('Ctrl Pts',(-20.4990934454001,24.5878317038046,-65.7462893152019));
#9931=CARTESIAN_POINT('Ctrl Pts',(-20.4974955196083,24.5831208355218,-65.7465834196329));
#9932=CARTESIAN_POINT('Ctrl Pts',(-20.4946397806468,24.5746372706644,-65.7471132361183));
#9933=CARTESIAN_POINT('Ctrl Pts',(-20.4933780294012,24.5708659035602,-65.7473488293377));
#9934=CARTESIAN_POINT('Ctrl Pts',(-20.4879152975852,24.5544368241394,-65.7483754271492));
#9935=CARTESIAN_POINT('Ctrl Pts',(-20.4837859731803,24.5417555657204,-65.7491685882956));
#9936=CARTESIAN_POINT('Ctrl Pts',(-20.4790081943181,24.5267675175551,-65.7501070623543));
#9937=CARTESIAN_POINT('Ctrl Pts',(-20.4782834089402,24.5244850533629,-65.7502500066031));
#9938=CARTESIAN_POINT('Ctrl Pts',(-20.476806263114,24.5198152486466,-65.7505425221624));
#9939=CARTESIAN_POINT('Ctrl Pts',(-20.4760541387286,24.5174278356541,-65.7506921006782));
#9940=CARTESIAN_POINT('Ctrl Pts',(-20.4733513365484,24.5088135246728,-65.7512319291571));
#9941=CARTESIAN_POINT('Ctrl Pts',(-20.4714167995651,24.5025816111569,-65.7516226802922));
#9942=CARTESIAN_POINT('Ctrl Pts',(-20.4675380249681,24.4899511820378,-65.7524150990565));
#9943=CARTESIAN_POINT('Ctrl Pts',(-20.4655947506359,24.4835524064316,-65.7528167946758));
#9944=CARTESIAN_POINT('Ctrl Pts',(-20.4558425973306,24.4510775221143,-65.7548567732224));
#9945=CARTESIAN_POINT('Ctrl Pts',(-20.4483445770606,24.4249098796529,-65.7565048206926));
#9946=CARTESIAN_POINT('Ctrl Pts',(-20.4389348735107,24.3904267205913,-65.7586832493702));
#9947=CARTESIAN_POINT('Ctrl Pts',(-20.4367233058081,24.3821936324742,-65.7592038590087));
#9948=CARTESIAN_POINT('Ctrl Pts',(-20.4334440470817,24.3697895771016,-65.7599889918));
#9949=CARTESIAN_POINT('Ctrl Pts',(-20.4323519930396,24.3656250412377,-65.7602527236829));
#9950=CARTESIAN_POINT('Ctrl Pts',(-20.4304213776608,24.358202068131,-65.7607230448587));
#9951=CARTESIAN_POINT('Ctrl Pts',(-20.4295795662572,24.3549444763286,-65.7609295284191));
#9952=CARTESIAN_POINT('Ctrl Pts',(-20.4278178390746,24.3480827073556,-65.7613646387786));
#9953=CARTESIAN_POINT('Ctrl Pts',(-20.4268990593167,24.3444782460052,-65.7615933020424));
#9954=CARTESIAN_POINT('Ctrl Pts',(-20.4244938665298,24.3349737241332,-65.7621965303873));
#9955=CARTESIAN_POINT('Ctrl Pts',(-20.4230179234487,24.3290710515639,-65.762571433735));
#9956=CARTESIAN_POINT('Ctrl Pts',(-20.4164659850116,24.3025492530772,-65.7642572089972));
#9957=CARTESIAN_POINT('Ctrl Pts',(-20.4115772316131,24.2818848184839,-65.7655741141248));
#9958=CARTESIAN_POINT('Ctrl Pts',(-20.3775478617192,24.1314229903325,-65.7751893818957));
#9959=CARTESIAN_POINT('Ctrl Pts',(-20.3562682103828,23.9999969096772,-65.7837398180584));
#9960=CARTESIAN_POINT('Ctrl Pts',(-20.3100028549861,23.5325117224265,-65.8146838240708));
#9961=CARTESIAN_POINT('Ctrl Pts',(-20.3295699811221,23.1942970741518,-65.8382653709866));
#9962=CARTESIAN_POINT('Ctrl Pts',(-20.4027425255166,22.8578977068628,-65.8602502824653));
#9963=CARTESIAN_POINT('Ctrl Pts',(-20.4043714099219,22.8505337220397,-65.8607306730568));
#9964=CARTESIAN_POINT('Ctrl Pts',(-20.4097524865003,22.8266051811846,-65.8622886669215));
#9965=CARTESIAN_POINT('Ctrl Pts',(-20.4136098529752,22.8100642061375,-65.8633609919435));
#9966=CARTESIAN_POINT('Ctrl Pts',(-20.4191689596851,22.7870500697052,-65.8648457123287));
#9967=CARTESIAN_POINT('Ctrl Pts',(-20.420760284114,22.7805508965555,-65.8652641874501));
#9968=CARTESIAN_POINT('Ctrl Pts',(-20.4229794705685,22.771608114635,-65.8658388444892));
#9969=CARTESIAN_POINT('Ctrl Pts',(-20.423589963603,22.7691602756424,-65.8659960211494));
#9970=CARTESIAN_POINT('Ctrl Pts',(-20.4246390301877,22.7649748654176,-65.8662645599438));
#9971=CARTESIAN_POINT('Ctrl Pts',(-20.4250761785647,22.763236943647,-65.8663760048269));
#9972=CARTESIAN_POINT('Ctrl Pts',(-20.4259548714067,22.7597558992927,-65.8665991038513));
#9973=CARTESIAN_POINT('Ctrl Pts',(-20.4263964240286,22.7580127860818,-65.8667107567695));
#9974=CARTESIAN_POINT('Ctrl Pts',(-20.4274330822529,22.7539347215117,-65.8669718269298));
#9975=CARTESIAN_POINT('Ctrl Pts',(-20.4280293493357,22.7516000614312,-65.8671211762725));
#9976=CARTESIAN_POINT('Ctrl Pts',(-20.4298771717933,22.7443986820033,-65.8675815147821));
#9977=CARTESIAN_POINT('Ctrl Pts',(-20.431137499454,22.739534189604,-65.8678919954399));
#9978=CARTESIAN_POINT('Ctrl Pts',(-20.4340754326698,22.7283028983563,-65.8686077858909));
#9979=CARTESIAN_POINT('Ctrl Pts',(-20.435761188543,22.7219382269582,-65.869012632014));
#9980=CARTESIAN_POINT('Ctrl Pts',(-20.441449185863,22.700725726665,-65.8703594374309));
#9981=CARTESIAN_POINT('Ctrl Pts',(-20.4455382637657,22.685901115199,-65.8712965993889));
#9982=CARTESIAN_POINT('Ctrl Pts',(-20.4629614035547,22.6244542719402,-65.8751663025215));
#9983=CARTESIAN_POINT('Ctrl Pts',(-20.4772414281265,22.5781042752581,-65.8780498780985));
#9984=CARTESIAN_POINT('Ctrl Pts',(-20.5389797959708,22.3926947160612,-65.8895068709393));
#9985=CARTESIAN_POINT('Ctrl Pts',(-20.5948789207734,22.2566228790572,-65.897741778693));
#9986=CARTESIAN_POINT('Ctrl Pts',(-20.7847719916005,21.8715696983216,-65.9217438131538));
#9987=CARTESIAN_POINT('Ctrl Pts',(-20.9423913826442,21.6358614309835,-65.9374685357283));
#9988=CARTESIAN_POINT('Ctrl Pts',(-21.1407510656897,21.4099828887004,-65.955670756922));
#9989=CARTESIAN_POINT('Ctrl Pts',(-21.1529248049126,21.3963557819931,-65.9567819539234));
#9990=CARTESIAN_POINT('Ctrl Pts',(-21.1692401192267,21.378402329817,-65.9582637219795));
#9991=CARTESIAN_POINT('Ctrl Pts',(-21.173278976214,21.3739827590094,-65.958629935503));
#9992=CARTESIAN_POINT('Ctrl Pts',(-21.1795821034396,21.3671239601925,-65.9592005396602));
#9993=CARTESIAN_POINT('Ctrl Pts',(-21.1818378910468,21.3646769258317,-65.9594045681934));
#9994=CARTESIAN_POINT('Ctrl Pts',(-21.1863492710179,21.359798255239,-65.9598122482485));
#9995=CARTESIAN_POINT('Ctrl Pts',(-21.1886048347874,21.3573665978977,-65.9600158984176));
#9996=CARTESIAN_POINT('Ctrl Pts',(-21.1936789662507,21.3519132339002,-65.9604736336871));
#9997=CARTESIAN_POINT('Ctrl Pts',(-21.1964995960121,21.3488934616907,-65.9607278072272));
#9998=CARTESIAN_POINT('Ctrl Pts',(-21.2047790164483,21.34006360144,-65.9614730896347));
#9999=CARTESIAN_POINT('Ctrl Pts',(-21.2102535380461,21.3342683652269,-65.9619648768608));
#10000=CARTESIAN_POINT('Ctrl Pts',(-21.2509461260023,21.291510815117,-65.9656130413122));
#10001=CARTESIAN_POINT('Ctrl Pts',(-21.2870148672163,21.2553715151228,-65.9688063904725));
#10002=CARTESIAN_POINT('Ctrl Pts',(-21.4084251449381,21.1393706575511,-65.9794345358521));
#10003=CARTESIAN_POINT('Ctrl Pts',(-21.4972448554269,21.0633005525426,-65.9870254776888));
#10004=CARTESIAN_POINT('Ctrl Pts',(-21.6948135121426,20.9119000134298,-66.0035107328305));
#10005=CARTESIAN_POINT('Ctrl Pts',(-21.8044689970814,20.8380958430611,-66.0124321525728));
#10006=CARTESIAN_POINT('Ctrl Pts',(-22.0707516512634,20.6817274270887,-66.0333355275552));
#10007=CARTESIAN_POINT('Ctrl Pts',(-22.2302872335823,20.6049066836124,-66.045303181188));
#10008=CARTESIAN_POINT('Ctrl Pts',(-22.4300574065046,20.5282227347728,-66.0590615162919));
#10009=CARTESIAN_POINT('Ctrl Pts',(-22.4650143350972,20.5154939636604,-66.0614248896733));
#10010=CARTESIAN_POINT('Ctrl Pts',(-22.5050555433346,20.501694290353,-66.0640757901158));
#10011=CARTESIAN_POINT('Ctrl Pts',(-22.5099295052411,20.5000276060807,-66.0643975261929));
#10012=CARTESIAN_POINT('Ctrl Pts',(-22.517131587097,20.4975840761345,-66.0648715336559));
#10013=CARTESIAN_POINT('Ctrl Pts',(-22.5194566011791,20.4967982033205,-66.0650243385446));
#10014=CARTESIAN_POINT('Ctrl Pts',(-22.5235707180809,20.4954128343725,-66.0652943410553));
#10015=CARTESIAN_POINT('Ctrl Pts',(-22.5253594508772,20.4948122531575,-66.0654116035372));
#10016=CARTESIAN_POINT('Ctrl Pts',(-22.5290530172931,20.4935757173974,-66.065653472307));
#10017=CARTESIAN_POINT('Ctrl Pts',(-22.5309579138164,20.4929399736964,-66.065778065796));
#10018=CARTESIAN_POINT('Ctrl Pts',(-22.5358890336922,20.4912993734819,-66.0661002196831));
#10019=CARTESIAN_POINT('Ctrl Pts',(-22.5389161657091,20.4902972239713,-66.0662976186808));
#10020=CARTESIAN_POINT('Ctrl Pts',(-22.5514977740422,20.4861527195812,-66.0671165643373));
#10021=CARTESIAN_POINT('Ctrl Pts',(-22.561065581394,20.4830505643916,-66.0677357492925));
#10022=CARTESIAN_POINT('Ctrl Pts',(-22.5857110550573,20.4751871178672,-66.0693218486954));
#10023=CARTESIAN_POINT('Ctrl Pts',(-22.6008097165177,20.4704918391863,-66.0702850638));
#10024=CARTESIAN_POINT('Ctrl Pts',(-22.6639183367668,20.4513749728996,-66.0742781350361));
#10025=CARTESIAN_POINT('Ctrl Pts',(-22.7122294534766,20.4379626433799,-66.0772557738976));
#10026=CARTESIAN_POINT('Ctrl Pts',(-22.8595246362911,20.4007488352297,-66.0861504968));
#10027=CARTESIAN_POINT('Ctrl Pts',(-22.9593455613922,20.380503276868,-66.0919309632075));
#10028=CARTESIAN_POINT('Ctrl Pts',(-23.3140806539183,20.3259005098677,-66.1121118656555));
#10029=CARTESIAN_POINT('Ctrl Pts',(-23.571945409682,20.3173364810395,-66.126215567801));
#10030=CARTESIAN_POINT('Ctrl Pts',(-23.8399061240362,20.3405237078021,-66.1420030143103));
#10031=CARTESIAN_POINT('Ctrl Pts',(-23.8517205064034,20.3416117942996,-66.1427011968122));
#10032=CARTESIAN_POINT('Ctrl Pts',(-23.9316858338088,20.3494220246755,-66.1474418281404));
#10033=CARTESIAN_POINT('Ctrl Pts',(-23.9996093862104,20.3582492963055,-66.1515429766519));
#10034=CARTESIAN_POINT('Ctrl Pts',(-24.0764933518689,20.3707436273136,-66.1562873932975));
#10035=CARTESIAN_POINT('Ctrl Pts',(-24.0857833166872,20.3722951611156,-66.1568623643496));
#10036=CARTESIAN_POINT('Ctrl Pts',(-24.0993785171449,20.3746270252545,-66.1577063259992));
#10037=CARTESIAN_POINT('Ctrl Pts',(-24.1036892369134,20.3753754446144,-66.1579742998851));
#10038=CARTESIAN_POINT('Ctrl Pts',(-24.1113316772106,20.3767183489973,-66.1584500560234));
#10039=CARTESIAN_POINT('Ctrl Pts',(-24.1146640170896,20.3773093094959,-66.1586577256299));
#10040=CARTESIAN_POINT('Ctrl Pts',(-24.121588153071,20.378548495774,-66.1590897048721));
#10041=CARTESIAN_POINT('Ctrl Pts',(-24.1251797895836,20.3791975760544,-66.1593140415018));
#10042=CARTESIAN_POINT('Ctrl Pts',(-24.1344481520235,20.3808888177802,-66.1598936355988));
#10043=CARTESIAN_POINT('Ctrl Pts',(-24.1401231768074,20.3819401267652,-66.1602491847034));
#10044=CARTESIAN_POINT('Ctrl Pts',(-24.1638723088497,20.3864057176512,-66.161739906545));
#10045=CARTESIAN_POINT('Ctrl Pts',(-24.1819195591316,20.389959406442,-66.1628795269972));
#10046=CARTESIAN_POINT('Ctrl Pts',(-24.3032099581798,20.4149231737606,-66.170585531538));
#10047=CARTESIAN_POINT('Ctrl Pts',(-24.405368485011,20.4412321678718,-66.1773087506991));
#10048=CARTESIAN_POINT('Ctrl Pts',(-24.6547413008138,20.5186745718332,-66.1943193529348));
#10049=CARTESIAN_POINT('Ctrl Pts',(-24.7998807766709,20.5755625238544,-66.2047630940263));
#10050=CARTESIAN_POINT('Ctrl Pts',(-25.0028633048507,20.6726069380651,-66.2199794332023));
#10051=CARTESIAN_POINT('Ctrl Pts',(-25.0644187029652,20.7045148265419,-66.2246779580549));
#10052=CARTESIAN_POINT('Ctrl Pts',(-25.206141098889,20.7838792607388,-66.2356422694246));
#10053=CARTESIAN_POINT('Ctrl Pts',(-25.2853796834973,20.8328781048237,-66.2418879669155));
#10054=CARTESIAN_POINT('Ctrl Pts',(-25.3926250637381,20.9058021274034,-66.2504062796723));
#10055=CARTESIAN_POINT('Ctrl Pts',(-25.4225103783518,20.9268758398528,-66.2527872470204));
#10056=CARTESIAN_POINT('Ctrl Pts',(-25.4837002505563,20.9716024577889,-66.257667125981));
#10057=CARTESIAN_POINT('Ctrl Pts',(-25.5149452784734,20.9953280625822,-66.2601616461832));
#10058=CARTESIAN_POINT('Ctrl Pts',(-25.5494961172242,21.0225726874404,-66.2629159636358));
#10059=CARTESIAN_POINT('Ctrl Pts',(-25.5532346819891,21.0255341680693,-66.2632139383201));
#10060=CARTESIAN_POINT('Ctrl Pts',(-25.5588521147189,21.0300043130716,-66.2636615627419));
#10061=CARTESIAN_POINT('Ctrl Pts',(-25.5607358665872,21.0315067865647,-66.2638116520133));
#10062=CARTESIAN_POINT('Ctrl Pts',(-25.5639942325197,21.0341116315058,-66.2640712320745));
#10063=CARTESIAN_POINT('Ctrl Pts',(-25.5653696272736,21.0352130174156,-66.2641807938175));
#10064=CARTESIAN_POINT('Ctrl Pts',(-25.5681310488031,21.0374280225238,-66.2644007427861));
#10065=CARTESIAN_POINT('Ctrl Pts',(-25.5695170553419,21.0385416591516,-66.2645111280591));
#10066=CARTESIAN_POINT('Ctrl Pts',(-25.5723534726861,21.0408245455266,-66.2647370068496));
#10067=CARTESIAN_POINT('Ctrl Pts',(-25.5738037945885,21.0419939087044,-66.2648524923042));
#10068=CARTESIAN_POINT('Ctrl Pts',(-25.57864300849,21.0459025911811,-66.2652377920346));
#10069=CARTESIAN_POINT('Ctrl Pts',(-25.5820273777565,21.0486475416243,-66.265507199849));
#10070=CARTESIAN_POINT('Ctrl Pts',(-25.6060157837334,21.0681845408122,-66.2674164433851));
#10071=CARTESIAN_POINT('Ctrl Pts',(-25.6264177371056,21.0852247001698,-66.2690385671186));
#10072=CARTESIAN_POINT('Ctrl Pts',(-25.6730770170003,21.1251858655287,-66.2727507111292));
#10073=CARTESIAN_POINT('Ctrl Pts',(-25.6991783890386,21.1482845889815,-66.27482906605));
#10074=CARTESIAN_POINT('Ctrl Pts',(-25.7725620408777,21.2153802554537,-66.2806947291003));
#10075=CARTESIAN_POINT('Ctrl Pts',(-25.8189051876307,21.2603826319328,-66.2844264779381));
#10076=CARTESIAN_POINT('Ctrl Pts',(-26.0745311943659,21.5239971977784,-66.3053840845503));
#10077=CARTESIAN_POINT('Ctrl Pts',(-26.2535431578115,21.7698241700775,-66.3217040956676));
#10078=CARTESIAN_POINT('Ctrl Pts',(-26.4051554223153,22.0549072981952,-66.3406220550871));
#10079=CARTESIAN_POINT('Ctrl Pts',(-26.4144977344831,22.0728807858263,-66.3418139457116));
#10080=CARTESIAN_POINT('Ctrl Pts',(-26.4258066511183,22.0951482958974,-66.3432901972283));
#10081=CARTESIAN_POINT('Ctrl Pts',(-26.4279342034909,22.099360383308,-66.3435694252613));
#10082=CARTESIAN_POINT('Ctrl Pts',(-26.4318681338264,22.1071913952035,-66.3440885380035));
#10083=CARTESIAN_POINT('Ctrl Pts',(-26.4336769668516,22.1108090806933,-66.3443283436209));
#10084=CARTESIAN_POINT('Ctrl Pts',(-26.4371462630953,22.1177804898347,-66.3447904483801));
#10085=CARTESIAN_POINT('Ctrl Pts',(-26.4388077053942,22.1211337208757,-66.3450127155576));
#10086=CARTESIAN_POINT('Ctrl Pts',(-26.4638910142021,22.1719809263763,-66.3483830766325));
#10087=CARTESIAN_POINT('Ctrl Pts',(-26.4861435033679,22.2200399450037,-66.3515685704321));
#10088=CARTESIAN_POINT('Ctrl Pts',(-26.5106740174188,22.2766362400392,-66.3553276249764));
#10089=CARTESIAN_POINT('Ctrl Pts',(-26.5141144452889,22.2846631882311,-66.3558609368523));
#10090=CARTESIAN_POINT('Ctrl Pts',(-26.5191954788754,22.2966522255265,-66.3566577816941));
#10091=CARTESIAN_POINT('Ctrl Pts',(-26.5208608916696,22.300603812012,-66.3569204686973));
#10092=CARTESIAN_POINT('Ctrl Pts',(-26.523818141712,22.3076599064786,-66.3573896203881));
#10093=CARTESIAN_POINT('Ctrl Pts',(-26.525113018785,22.3107631402389,-66.3575959812947));
#10094=CARTESIAN_POINT('Ctrl Pts',(-26.5278336764274,22.3173121457651,-66.3580315481102));
#10095=CARTESIAN_POINT('Ctrl Pts',(-26.5292583368283,22.3207583749303,-66.3582607917057));
#10096=CARTESIAN_POINT('Ctrl Pts',(-26.5330076616705,22.3298727020612,-66.3588671847354));
#10097=CARTESIAN_POINT('Ctrl Pts',(-26.5353221426211,22.3355449491599,-66.3592446788801));
#10098=CARTESIAN_POINT('Ctrl Pts',(-26.5457402824454,22.3612869466681,-66.3609583607167));
#10099=CARTESIAN_POINT('Ctrl Pts',(-26.553657653799,22.3814310470441,-66.3623008296803));
#10100=CARTESIAN_POINT('Ctrl Pts',(-26.6103284194216,22.5299966716802,-66.3722141645426));
#10101=CARTESIAN_POINT('Ctrl Pts',(-26.6510232232312,22.6613213713506,-66.3810542451801));
#10102=CARTESIAN_POINT('Ctrl Pts',(-26.7430104087554,23.042817882465,-66.4069449877869));
#10103=CARTESIAN_POINT('Ctrl Pts',(-26.7731425913759,23.2969902927874,-66.424513397672));
#10104=CARTESIAN_POINT('Ctrl Pts',(-26.7730020423193,23.5520285569696,-66.4414562157347));
#10105=CARTESIAN_POINT('Ctrl Pts',(-26.773002039719,23.5520332692001,-66.4414565287797));
#10106=CARTESIAN_POINT('Ctrl Pts',(-26.7729453408972,23.6546458662236,-66.4482733316772));
#10107=CARTESIAN_POINT('Ctrl Pts',(-26.7679878384078,23.7572120994706,-66.4549625706889));
#10108=CARTESIAN_POINT('Ctrl Pts',(-26.7577653228673,23.8632936085473,-66.4616370519691));
#10109=CARTESIAN_POINT('Ctrl Pts',(-26.757381021648,23.8672065830185,-66.4618829019462));
#10110=CARTESIAN_POINT('Ctrl Pts',(-26.7567442964397,23.8735700124737,-66.4622821353406));
#10111=CARTESIAN_POINT('Ctrl Pts',(-26.7564962235519,23.8760208838679,-66.4624357605224));
#10112=CARTESIAN_POINT('Ctrl Pts',(-26.7560555759835,23.8803250623757,-66.4627053067962));
#10113=CARTESIAN_POINT('Ctrl Pts',(-26.7558642041094,23.8821784872966,-66.4628212956041));
#10114=CARTESIAN_POINT('Ctrl Pts',(-26.7554870989613,23.8857999826482,-66.4630477726126));
#10115=CARTESIAN_POINT('Ctrl Pts',(-26.7553015096936,23.8875680690343,-66.4631582690861));
#10116=CARTESIAN_POINT('Ctrl Pts',(-26.7549290923121,23.8910879877591,-66.4633780975537));
#10117=CARTESIAN_POINT('Ctrl Pts',(-26.7547422910305,23.8928398178431,-66.463487430893));
#10118=CARTESIAN_POINT('Ctrl Pts',(-26.7542967143381,23.8969862032602,-66.4637460392282));
#10119=CARTESIAN_POINT('Ctrl Pts',(-26.7540366904872,23.8993806275095,-66.4638952431161));
#10120=CARTESIAN_POINT('Ctrl Pts',(-26.7532542130701,23.9065115652908,-66.4643391964043));
#10121=CARTESIAN_POINT('Ctrl Pts',(-26.7527239352616,23.911247240711,-66.4646335048976));
#10122=CARTESIAN_POINT('Ctrl Pts',(-26.7477451243082,23.9548363390854,-66.4673377762807));
#10123=CARTESIAN_POINT('Ctrl Pts',(-26.7425999836289,23.9936090700557,-66.4697091109559));
#10124=CARTESIAN_POINT('Ctrl Pts',(-26.7355098906049,24.0404788765626,-66.4725446296912));
#10125=CARTESIAN_POINT('Ctrl Pts',(-26.7342380786684,24.0486723859798,-66.4730391648288));
#10126=CARTESIAN_POINT('Ctrl Pts',(-26.7313480841914,24.0668282888138,-66.4741326202887));
#10127=CARTESIAN_POINT('Ctrl Pts',(-26.7297146897169,24.0767882070042,-66.4747308744348));
#10128=CARTESIAN_POINT('Ctrl Pts',(-26.727341744739,24.0908438869464,-66.4755731037343));
#10129=CARTESIAN_POINT('Ctrl Pts',(-26.7266410245999,24.0949460450309,-66.4758186628769));
#10130=CARTESIAN_POINT('Ctrl Pts',(-26.7201860629443,24.1322986390939,-66.478052477427));
#10131=CARTESIAN_POINT('Ctrl Pts',(-26.7139176772514,24.1654592102627,-66.4800200952918));
#10132=CARTESIAN_POINT('Ctrl Pts',(-26.7044914802644,24.2113623554518,-66.4827297176055));
#10133=CARTESIAN_POINT('Ctrl Pts',(-26.7017751219382,24.2241923762255,-66.4834855241049));
#10134=CARTESIAN_POINT('Ctrl Pts',(-26.6390657724993,24.5117115652518,-66.5003954752968));
#10135=CARTESIAN_POINT('Ctrl Pts',(-26.5434612698304,24.7773993447194,-66.5155679285083));
#10136=CARTESIAN_POINT('Ctrl Pts',(-26.376986752372,25.1002267167793,-66.5365304372054));
#10137=CARTESIAN_POINT('Ctrl Pts',(-26.3366234921934,25.1716659909652,-66.5413367737022));
#10138=CARTESIAN_POINT('Ctrl Pts',(-26.2710478810099,25.2780355051333,-66.5488054443128));
#10139=CARTESIAN_POINT('Ctrl Pts',(-26.2477869291491,25.3141315637175,-66.5513971652073));
#10140=CARTESIAN_POINT('Ctrl Pts',(-26.2195594424802,25.3560698529034,-66.5544805910169));
#10141=CARTESIAN_POINT('Ctrl Pts',(-26.2152839379331,25.3623737152076,-66.5549460232644));
#10142=CARTESIAN_POINT('Ctrl Pts',(-26.2086969698946,25.3720118987769,-66.5556606631608));
#10143=CARTESIAN_POINT('Ctrl Pts',(-26.2064014709131,25.3753571410242,-66.5559092632962));
#10144=CARTESIAN_POINT('Ctrl Pts',(-26.2023867056021,25.3811842621792,-66.5563432872559));
#10145=CARTESIAN_POINT('Ctrl Pts',(-26.2006702533382,25.3836680816462,-66.5565286035318));
#10146=CARTESIAN_POINT('Ctrl Pts',(-26.19680155733,25.3892495531813,-66.5569457401907));
#10147=CARTESIAN_POINT('Ctrl Pts',(-26.1946473633074,25.3923458421638,-66.5571776350067));
#10148=CARTESIAN_POINT('Ctrl Pts',(-26.1888705756707,25.4006179802422,-66.5577984906114));
#10149=CARTESIAN_POINT('Ctrl Pts',(-26.1852382035554,25.4057869515729,-66.5581878261843));
#10150=CARTESIAN_POINT('Ctrl Pts',(-26.1695086725674,25.4280312028943,-66.5598693147173));
#10151=CARTESIAN_POINT('Ctrl Pts',(-26.1572607752796,25.4449988086725,-66.5611672692849));
#10152=CARTESIAN_POINT('Ctrl Pts',(-25.9337053533548,25.7484295194022,-66.5846607650994));
#10153=CARTESIAN_POINT('Ctrl Pts',(-25.676572082334,25.9979976636996,-66.6089625633056));
#10154=CARTESIAN_POINT('Ctrl Pts',(-25.3279889752494,26.2391949593515,-66.6374318425259));
#10155=CARTESIAN_POINT('Ctrl Pts',(-25.2707514854744,26.2761730262208,-66.6419713430421));
#10156=CARTESIAN_POINT('Ctrl Pts',(-25.1694340936191,26.3371650924372,-66.6497264723703));
#10157=CARTESIAN_POINT('Ctrl Pts',(-25.125885855192,26.3620154657123,-66.6529739212147));
#10158=CARTESIAN_POINT('Ctrl Pts',(-25.0607045202194,26.3972203434076,-66.6576902154815));
#10159=CARTESIAN_POINT('Ctrl Pts',(-25.0395090954947,26.4083648283991,-66.6592018269723));
#10160=CARTESIAN_POINT('Ctrl Pts',(-25.0144197383457,26.4212018339314,-66.6609636389405));
#10161=CARTESIAN_POINT('Ctrl Pts',(-25.010644977508,26.4231238148793,-66.6612279811058));
#10162=CARTESIAN_POINT('Ctrl Pts',(-25.0052160457243,26.4258745788889,-66.6616071072701));
#10163=CARTESIAN_POINT('Ctrl Pts',(-25.003564954101,26.4267093779533,-66.6617222702242));
#10164=CARTESIAN_POINT('Ctrl Pts',(-25.00031708957,26.428348002016,-66.6619485308413));
#10165=CARTESIAN_POINT('Ctrl Pts',(-24.9987203637366,26.429151921721,-66.662059634519));
#10166=CARTESIAN_POINT('Ctrl Pts',(-24.9955353820572,26.4307521761328,-66.6622809898053));
#10167=CARTESIAN_POINT('Ctrl Pts',(-24.9939471399595,26.4315485243455,-66.6623912422478));
#10168=CARTESIAN_POINT('Ctrl Pts',(-24.9901533199767,26.433446829909,-66.6626542931486));
#10169=CARTESIAN_POINT('Ctrl Pts',(-24.9879471305079,26.4345475724262,-66.6628070145965));
#10170=CARTESIAN_POINT('Ctrl Pts',(-24.9800633065217,26.4384697857764,-66.663351886097));
#10171=CARTESIAN_POINT('Ctrl Pts',(-24.974378563609,26.4412770569157,-66.6637431469159));
#10172=CARTESIAN_POINT('Ctrl Pts',(-24.8918941259207,26.4817076462584,-66.6693972598639));
#10173=CARTESIAN_POINT('Ctrl Pts',(-24.8136267525672,26.5162801565671,-66.6744740813416));
#10174=CARTESIAN_POINT('Ctrl Pts',(-24.6025077453349,26.5996597796819,-66.6876543849707));
#10175=CARTESIAN_POINT('Ctrl Pts',(-24.4676593107816,26.6429044493942,-66.69555659579));
#10176=CARTESIAN_POINT('Ctrl Pts',(-24.3142149719278,26.6811880368407,-66.7043937341486));
#10177=CARTESIAN_POINT('Ctrl Pts',(-24.2980010643669,26.6850998771355,-66.7053255507264));
#10178=CARTESIAN_POINT('Ctrl Pts',(-24.2630368230461,26.6932488120214,-66.7073318557541));
#10179=CARTESIAN_POINT('Ctrl Pts',(-24.2442774937518,26.697444361483,-66.7084063896779));
#10180=CARTESIAN_POINT('Ctrl Pts',(-24.2034822227336,26.7061857907588,-66.7107407057408));
#10181=CARTESIAN_POINT('Ctrl Pts',(-24.1814339920301,26.7106692321189,-66.7120007781898));
#10182=CARTESIAN_POINT('Ctrl Pts',(-24.1328804434403,26.7200140938005,-66.7147749112308));
#10183=CARTESIAN_POINT('Ctrl Pts',(-24.106357555101,26.7247746726938,-66.7162898339661));
#10184=CARTESIAN_POINT('Ctrl Pts',(-24.0466927892136,26.7347131857336,-66.7197010010988));
#10185=CARTESIAN_POINT('Ctrl Pts',(-24.0135237376521,26.7397073930787,-66.7215996065667));
#10186=CARTESIAN_POINT('Ctrl Pts',(-23.8804282414592,26.7576273676666,-66.7292407186346));
#10187=CARTESIAN_POINT('Ctrl Pts',(-23.7800051021913,26.7663807234197,-66.735059358282));
#10188=CARTESIAN_POINT('Ctrl Pts',(-23.6147561657635,26.7730052297384,-66.7448407972053));
#10189=CARTESIAN_POINT('Ctrl Pts',(-23.5501103046843,26.7736505448982,-66.7487184468738));
#10190=CARTESIAN_POINT('Ctrl Pts',(-23.4770650262638,26.7721824183442,-66.7531718122301));
#10191=CARTESIAN_POINT('Ctrl Pts',(-23.4686387915671,26.7719799876928,-66.7536866106322));
#10192=CARTESIAN_POINT('Ctrl Pts',(-23.4559885567267,26.771626420224,-66.7544611180973));
#10193=CARTESIAN_POINT('Ctrl Pts',(-23.4517638553899,26.7715000240565,-66.7547200498865));
#10194=CARTESIAN_POINT('Ctrl Pts',(-23.4445007075638,26.77126842073,-66.7551656859412));
#10195=CARTESIAN_POINT('Ctrl Pts',(-23.4414621313609,26.7711672238925,-66.7553522639929));
#10196=CARTESIAN_POINT('Ctrl Pts',(-23.4352067928245,26.7709500340231,-66.755736659301));
#10197=CARTESIAN_POINT('Ctrl Pts',(-23.4319900526409,26.7708335211216,-66.7559344927059));
#10198=CARTESIAN_POINT('Ctrl Pts',(-23.4242498800362,26.7705415539009,-66.7564109156523));
#10199=CARTESIAN_POINT('Ctrl Pts',(-23.419726640974,26.7703613879747,-66.7566896530004));
#10200=CARTESIAN_POINT('Ctrl Pts',(-23.4058572920852,26.7697796846202,-66.7575453284505));
#10201=CARTESIAN_POINT('Ctrl Pts',(-23.3965126011422,26.7693469857978,-66.7581232448087));
#10202=CARTESIAN_POINT('Ctrl Pts',(-23.2882485258053,26.7638614133981,-66.76483515588));
#10203=CARTESIAN_POINT('Ctrl Pts',(-23.1896206564721,26.7542920622106,-66.7711108041114));
#10204=CARTESIAN_POINT('Ctrl Pts',(-22.8029283642046,26.6986929285994,-66.7963919260849));
#10205=CARTESIAN_POINT('Ctrl Pts',(-22.5212493860532,26.6181952366371,-66.8164604755562));
#10206=CARTESIAN_POINT('Ctrl Pts',(-22.1936910076554,26.474332169919,-66.8403569096297));
#10207=CARTESIAN_POINT('Ctrl Pts',(-22.1339047982687,26.4458458795231,-66.8447348211984));
#10208=CARTESIAN_POINT('Ctrl Pts',(-22.0750360151859,26.4155367744738,-66.8490341587423));
#10209=CARTESIAN_POINT('',(-26.7730013023275,23.5474375926689,-66.6850863746791));
#10210=CARTESIAN_POINT('Ctrl Pts',(-22.0750362583504,26.4155368996692,-67.093261398997));
#10211=CARTESIAN_POINT('Ctrl Pts',(-22.1505511773086,26.4544164044654,-67.0875238249795));
#10212=CARTESIAN_POINT('Ctrl Pts',(-22.2276018483777,26.4903099549655,-67.081759723405));
#10213=CARTESIAN_POINT('Ctrl Pts',(-22.4545604981318,26.5852993095174,-67.0651565858544));
#10214=CARTESIAN_POINT('Ctrl Pts',(-22.6075825615071,26.6362592309213,-67.0544127197646));
#10215=CARTESIAN_POINT('Ctrl Pts',(-22.7729459163076,26.6778716094321,-67.0436883118301));
#10216=CARTESIAN_POINT('Ctrl Pts',(-22.7821104012551,26.6801350123157,-67.0430968116143));
#10217=CARTESIAN_POINT('Ctrl Pts',(-22.7944278757522,26.6831197664715,-67.0423057540625));
#10218=CARTESIAN_POINT('Ctrl Pts',(-22.7975720783738,26.6838766566779,-67.0421041703756));
#10219=CARTESIAN_POINT('Ctrl Pts',(-22.8024997567178,26.6850550307932,-67.0417887883655));
#10220=CARTESIAN_POINT('Ctrl Pts',(-22.804282450609,26.6854797258555,-67.0416748038514));
#10221=CARTESIAN_POINT('Ctrl Pts',(-22.8077067710442,26.6862924232297,-67.0414560704241));
#10222=CARTESIAN_POINT('Ctrl Pts',(-22.8093483292713,26.6866806547044,-67.0413513088939));
#10223=CARTESIAN_POINT('Ctrl Pts',(-22.8127379548925,26.6874794976309,-67.0411351847337));
#10224=CARTESIAN_POINT('Ctrl Pts',(-22.8144860554825,26.6878899357478,-67.0410238325259));
#10225=CARTESIAN_POINT('Ctrl Pts',(-22.8184329611372,26.6888131534297,-67.0407726595012));
#10226=CARTESIAN_POINT('Ctrl Pts',(-22.8206319667729,26.6893250844523,-67.0406328878849));
#10227=CARTESIAN_POINT('Ctrl Pts',(-22.8309752453531,26.6917215556337,-67.0399762407764));
#10228=CARTESIAN_POINT('Ctrl Pts',(-22.8391263914278,26.6935767369449,-67.0394610496647));
#10229=CARTESIAN_POINT('Ctrl Pts',(-22.9289550481959,26.7136542201972,-67.0338076922075));
#10230=CARTESIAN_POINT('Ctrl Pts',(-23.0113137464413,26.7287220701921,-67.0288446981667));
#10231=CARTESIAN_POINT('Ctrl Pts',(-23.2287302703402,26.759803361815,-67.0160970370804));
#10232=CARTESIAN_POINT('Ctrl Pts',(-23.3643784978459,26.770508558548,-67.0084934787041));
#10233=CARTESIAN_POINT('Ctrl Pts',(-23.7762002888445,26.7768919030031,-66.9854753483792));
#10234=CARTESIAN_POINT('Ctrl Pts',(-24.0514568117553,26.7457215561494,-66.970068567576));
#10235=CARTESIAN_POINT('Ctrl Pts',(-24.3367278049164,26.6756155225269,-66.952277087987));
#10236=CARTESIAN_POINT('Ctrl Pts',(-24.3540529920767,26.6712046267555,-66.9511897530952));
#10237=CARTESIAN_POINT('Ctrl Pts',(-24.3770792246922,26.6651378271145,-66.9497352341898));
#10238=CARTESIAN_POINT('Ctrl Pts',(-24.3828139161051,26.6636099355787,-66.9493722078512));
#10239=CARTESIAN_POINT('Ctrl Pts',(-24.3917478585975,26.6612032199407,-66.9488054328442));
#10240=CARTESIAN_POINT('Ctrl Pts',(-24.3949500487826,26.6603352756729,-66.9486020381742));
#10241=CARTESIAN_POINT('Ctrl Pts',(-24.4013525614472,26.6585892758269,-66.9481948734571));
#10242=CARTESIAN_POINT('Ctrl Pts',(-24.4045528793908,26.657711218687,-66.9479911035682));
#10243=CARTESIAN_POINT('Ctrl Pts',(-24.41175498237,26.6557232425883,-66.947531973584));
#10244=CARTESIAN_POINT('Ctrl Pts',(-24.4157559841133,26.654610530111,-66.9472765227323));
#10245=CARTESIAN_POINT('Ctrl Pts',(-24.4275259390017,26.6513126831422,-66.9465238969655));
#10246=CARTESIAN_POINT('Ctrl Pts',(-24.4352888052014,26.649106107897,-66.9460260231885));
#10247=CARTESIAN_POINT('Ctrl Pts',(-24.4936154633616,26.632289858447,-66.9422739699456));
#10248=CARTESIAN_POINT('Ctrl Pts',(-24.5438203103723,26.6164733724153,-66.9389804651138));
#10249=CARTESIAN_POINT('Ctrl Pts',(-24.7100091715604,26.5596073500084,-66.9278543266071));
#10250=CARTESIAN_POINT('Ctrl Pts',(-24.824015933098,26.5131518823701,-66.919847082871));
#10251=CARTESIAN_POINT('Ctrl Pts',(-25.005512358643,26.4267818297944,-66.9065035696559));
#10252=CARTESIAN_POINT('Ctrl Pts',(-25.0747034225353,26.3907191339648,-66.9012675710791));
#10253=CARTESIAN_POINT('Ctrl Pts',(-25.2106930926289,26.313439814816,-66.8907112468174));
#10254=CARTESIAN_POINT('Ctrl Pts',(-25.2774336891162,26.2722209251642,-66.885394020666));
#10255=CARTESIAN_POINT('Ctrl Pts',(-25.4688488739672,26.1441262433553,-66.8698251493757));
#10256=CARTESIAN_POINT('Ctrl Pts',(-25.5889768697811,26.0508135920372,-66.8596309255803));
#10257=CARTESIAN_POINT('Ctrl Pts',(-25.7042648428269,25.9474085780935,-66.8497218415432));
#10258=CARTESIAN_POINT('Ctrl Pts',(-25.7064433504623,25.9454492460579,-66.8495345518188));
#10259=CARTESIAN_POINT('Ctrl Pts',(-25.7139116372128,25.9387138836178,-66.8488923444932));
#10260=CARTESIAN_POINT('Ctrl Pts',(-25.7191882894192,25.9339232378656,-66.8484383448836));
#10261=CARTESIAN_POINT('Ctrl Pts',(-25.7261598639978,25.9275514644086,-66.8478382292061));
#10262=CARTESIAN_POINT('Ctrl Pts',(-25.7278689853072,25.9259860005958,-66.8476910845236));
#10263=CARTESIAN_POINT('Ctrl Pts',(-25.7435573817223,25.9115851142038,-66.8463402131384));
#10264=CARTESIAN_POINT('Ctrl Pts',(-25.7574251163073,25.8986279177598,-66.8451446625162));
#10265=CARTESIAN_POINT('Ctrl Pts',(-25.7739264696091,25.8829347147107,-66.8437211995362));
#10266=CARTESIAN_POINT('Ctrl Pts',(-25.7766703643264,25.8803159608796,-66.8434844728169));
#10267=CARTESIAN_POINT('Ctrl Pts',(-25.7811350492552,25.8760398098567,-66.8430992490486));
#10268=CARTESIAN_POINT('Ctrl Pts',(-25.7828586199841,25.8743853430946,-66.8429505260404));
#10269=CARTESIAN_POINT('Ctrl Pts',(-25.7859300859509,25.8714304533042,-66.8426854824972));
#10270=CARTESIAN_POINT('Ctrl Pts',(-25.787278685953,25.8701307732418,-66.84256910423));
#10271=CARTESIAN_POINT('Ctrl Pts',(-25.790140823725,25.867367641943,-66.8423221051491));
#10272=CARTESIAN_POINT('Ctrl Pts',(-25.7916540566739,25.8659038868856,-66.842191509194));
#10273=CARTESIAN_POINT('Ctrl Pts',(-25.7947366010381,25.8629162793644,-66.8419254630813));
#10274=CARTESIAN_POINT('Ctrl Pts',(-25.7963057978945,25.8613923095498,-66.841790022246));
#10275=CARTESIAN_POINT('Ctrl Pts',(-25.8002197033979,25.857583458769,-66.8414521814976));
#10276=CARTESIAN_POINT('Ctrl Pts',(-25.8025624908468,25.8552965939422,-66.8412499360102));
#10277=CARTESIAN_POINT('Ctrl Pts',(-25.8288512793811,25.8295569762198,-66.8389802186312));
#10278=CARTESIAN_POINT('Ctrl Pts',(-25.8524346391535,25.8057344679384,-66.8369413837415));
#10279=CARTESIAN_POINT('Ctrl Pts',(-25.9448069499592,25.7094667241729,-66.8289230946981));
#10280=CARTESIAN_POINT('Ctrl Pts',(-26.0105886562705,25.6342023148557,-66.8231386030559));
#10281=CARTESIAN_POINT('Ctrl Pts',(-26.1175374910903,25.4996983215217,-66.8133599100091));
#10282=CARTESIAN_POINT('Ctrl Pts',(-26.1604062637903,25.4419155598186,-66.8093210668536));
#10283=CARTESIAN_POINT('Ctrl Pts',(-26.2624073287804,25.2943513566348,-66.7992819542795));
#10284=CARTESIAN_POINT('Ctrl Pts',(-26.3190485158035,25.2029572239175,-66.7933030096132));
#10285=CARTESIAN_POINT('Ctrl Pts',(-26.4651265642402,24.9385932114365,-66.7762780167469));
#10286=CARTESIAN_POINT('Ctrl Pts',(-26.5436031744961,24.7601348511216,-66.7650648308309));
#10287=CARTESIAN_POINT('Ctrl Pts',(-26.609565460328,24.5636058144705,-66.7524691348085));
#10288=CARTESIAN_POINT('Ctrl Pts',(-26.6135547586185,24.5514817413134,-66.7516912805668));
#10289=CARTESIAN_POINT('Ctrl Pts',(-26.6188974329064,24.534913695648,-66.7506271004287));
#10290=CARTESIAN_POINT('Ctrl Pts',(-26.6203134144978,24.5304899075612,-66.7503428394148));
#10291=CARTESIAN_POINT('Ctrl Pts',(-26.6227042419424,24.5229645244729,-66.7498590731801));
#10292=CARTESIAN_POINT('Ctrl Pts',(-26.6236839701504,24.5198644776272,-66.7496597289118));
#10293=CARTESIAN_POINT('Ctrl Pts',(-26.6255676328128,24.5138726698851,-66.7492743178349));
#10294=CARTESIAN_POINT('Ctrl Pts',(-26.6264721839222,24.5109811057688,-66.7490882715864));
#10295=CARTESIAN_POINT('Ctrl Pts',(-26.6286055178869,24.5041276082937,-66.7486471848317));
#10296=CARTESIAN_POINT('Ctrl Pts',(-26.6298307293967,24.500164576748,-66.7483920273059));
#10297=CARTESIAN_POINT('Ctrl Pts',(-26.6334104416078,24.4885060314283,-66.7476411002953));
#10298=CARTESIAN_POINT('Ctrl Pts',(-26.6357437595273,24.4808040930317,-66.7471446367313));
#10299=CARTESIAN_POINT('Ctrl Pts',(-26.6409405476884,24.4634158110116,-66.7460229026759));
#10300=CARTESIAN_POINT('Ctrl Pts',(-26.6437873667097,24.4537246163261,-66.7453970915488));
#10301=CARTESIAN_POINT('Ctrl Pts',(-26.6527342900554,24.4227292253103,-66.7433934852256));
#10302=CARTESIAN_POINT('Ctrl Pts',(-26.6586601321783,24.4013757845281,-66.7420100313259));
#10303=CARTESIAN_POINT('Ctrl Pts',(-26.736743252748,24.1083102646871,-66.7229771510973));
#10304=CARTESIAN_POINT('Ctrl Pts',(-26.773246729524,23.8284206579786,-66.7041027857559));
#10305=CARTESIAN_POINT('Ctrl Pts',(-26.7730013023275,23.5474375926689,-66.6850863746791));
#10306=CARTESIAN_POINT('Ctrl Pts',(-26.7730013006479,23.5474356704599,-66.6850862445875));
#10307=CARTESIAN_POINT('Ctrl Pts',(-26.7728538349007,23.3787212695974,-66.673667968088));
#10308=CARTESIAN_POINT('Ctrl Pts',(-26.7594579767268,23.2102566127178,-66.6622840767911));
#10309=CARTESIAN_POINT('Ctrl Pts',(-26.7280225822497,23.012787796804,-66.6494702834752));
#10310=CARTESIAN_POINT('Ctrl Pts',(-26.7226706477898,22.9820498303895,-66.6474916045324));
#10311=CARTESIAN_POINT('Ctrl Pts',(-26.7161312057531,22.9474708818912,-66.645287346235));
#10312=CARTESIAN_POINT('Ctrl Pts',(-26.7153821662279,22.9435500566689,-66.6450377261054));
#10313=CARTESIAN_POINT('Ctrl Pts',(-26.7141543342157,22.9371871687715,-66.6446331552387));
#10314=CARTESIAN_POINT('Ctrl Pts',(-26.7136799973535,22.9347442662529,-66.644477953824));
#10315=CARTESIAN_POINT('Ctrl Pts',(-26.7128438051381,22.9304642569679,-66.6442062609315));
#10316=CARTESIAN_POINT('Ctrl Pts',(-26.7124831782526,22.9286269157797,-66.6440896994001));
#10317=CARTESIAN_POINT('Ctrl Pts',(-26.7117536539914,22.924927159698,-66.6438551321121));
#10318=CARTESIAN_POINT('Ctrl Pts',(-26.7113847112272,22.9230647522015,-66.6437371289139));
#10319=CARTESIAN_POINT('Ctrl Pts',(-26.7106675528228,22.9194612752106,-66.643508956589));
#10320=CARTESIAN_POINT('Ctrl Pts',(-26.710319545023,22.9177201717781,-66.6433987756693));
#10321=CARTESIAN_POINT('Ctrl Pts',(-26.7094857646807,22.9135665823217,-66.6431360824067));
#10322=CARTESIAN_POINT('Ctrl Pts',(-26.7089986665251,22.9111543590166,-66.6429836465839));
#10323=CARTESIAN_POINT('Ctrl Pts',(-26.7075189469428,22.9038694612276,-66.642523662486));
#10324=CARTESIAN_POINT('Ctrl Pts',(-26.7065178042862,22.8989984948894,-66.642216600866));
#10325=CARTESIAN_POINT('Ctrl Pts',(-26.6962380275353,22.8495636945561,-66.6391051889979));
#10326=CARTESIAN_POINT('Ctrl Pts',(-26.686026918792,22.8051960907119,-66.6363532880314));
#10327=CARTESIAN_POINT('Ctrl Pts',(-26.637757451749,22.6140849800131,-66.6246174541903));
#10328=CARTESIAN_POINT('Ctrl Pts',(-26.5903086846143,22.4698985209697,-66.6160611961401));
#10329=CARTESIAN_POINT('Ctrl Pts',(-26.521641441517,22.3021155781672,-66.6059073940391));
#10330=CARTESIAN_POINT('Ctrl Pts',(-26.5100244128222,22.274812085168,-66.604248796313));
#10331=CARTESIAN_POINT('Ctrl Pts',(-26.4874619147879,22.2237524324373,-66.6011293758084));
#10332=CARTESIAN_POINT('Ctrl Pts',(-26.4766010907327,22.1999616063984,-66.5996685506246));
#10333=CARTESIAN_POINT('Ctrl Pts',(-26.4427270397673,22.1280886597394,-66.5952267129182));
#10334=CARTESIAN_POINT('Ctrl Pts',(-26.4188096582066,22.0804434460837,-66.592242675412));
#10335=CARTESIAN_POINT('Ctrl Pts',(-26.3198391295674,21.8949130535386,-66.5804031420904));
#10336=CARTESIAN_POINT('Ctrl Pts',(-26.2359445814555,21.7620107835425,-66.5714197444653));
#10337=CARTESIAN_POINT('Ctrl Pts',(-26.1129226451039,21.595424292625,-66.5590871712984));
#10338=CARTESIAN_POINT('Ctrl Pts',(-26.0822009891195,21.5557931724937,-66.5560672680176));
#10339=CARTESIAN_POINT('Ctrl Pts',(-26.0455055930862,21.5106706833333,-66.5525210156025));
#10340=CARTESIAN_POINT('Ctrl Pts',(-26.0404193736614,21.504463917521,-66.5520307915641));
#10341=CARTESIAN_POINT('Ctrl Pts',(-26.0326719558048,21.4950813630937,-66.5512860229376));
#10342=CARTESIAN_POINT('Ctrl Pts',(-26.0300277006719,21.4918915719702,-66.551032168671));
#10343=CARTESIAN_POINT('Ctrl Pts',(-26.0252549730742,21.4861567283552,-66.5505745851002));
#10344=CARTESIAN_POINT('Ctrl Pts',(-26.0231287043421,21.4836098424959,-66.550370946086));
#10345=CARTESIAN_POINT('Ctrl Pts',(-26.0188651836227,21.4785189153098,-66.5499630458426));
#10346=CARTESIAN_POINT('Ctrl Pts',(-26.0167279226205,21.4759748867433,-66.5497587843827));
#10347=CARTESIAN_POINT('Ctrl Pts',(-26.0107465063935,21.4688773914026,-66.5491877269604));
#10348=CARTESIAN_POINT('Ctrl Pts',(-26.0068936646777,21.4643312922593,-66.5488205738133));
#10349=CARTESIAN_POINT('Ctrl Pts',(-25.9913131858863,21.4460503960531,-66.5473385733511));
#10350=CARTESIAN_POINT('Ctrl Pts',(-25.9794829726389,21.4324038146009,-66.546219487416));
#10351=CARTESIAN_POINT('Ctrl Pts',(-25.7832836150021,21.2098875543304,-66.5277581572107));
#10352=CARTESIAN_POINT('Ctrl Pts',(-25.5727500397149,21.025738507981,-66.5092005090331));
#10353=CARTESIAN_POINT('Ctrl Pts',(-25.278981920928,20.829366775303,-66.4852832238685));
#10354=CARTESIAN_POINT('Ctrl Pts',(-25.215297174336,20.7899352970996,-66.4802112787161));
#10355=CARTESIAN_POINT('Ctrl Pts',(-25.0726632541683,20.7083549988295,-66.4691622130525));
#10356=CARTESIAN_POINT('Ctrl Pts',(-24.993210110548,20.6672000431357,-66.4632050091617));
#10357=CARTESIAN_POINT('Ctrl Pts',(-24.8768208207622,20.6129318105343,-66.4548514764427));
#10358=CARTESIAN_POINT('Ctrl Pts',(-24.8412011801104,20.5971036461663,-66.4523434907402));
#10359=CARTESIAN_POINT('Ctrl Pts',(-24.793288737847,20.5768456212321,-66.4490424678556));
#10360=CARTESIAN_POINT('Ctrl Pts',(-24.7812450805936,20.5718393597389,-66.4482187339925));
#10361=CARTESIAN_POINT('Ctrl Pts',(-24.7611544469397,20.5636308432856,-66.4468550425463));
#10362=CARTESIAN_POINT('Ctrl Pts',(-24.7531244841774,20.5603877140049,-66.4463127469483));
#10363=CARTESIAN_POINT('Ctrl Pts',(-24.7429607553265,20.5563303767688,-66.4456299137494));
#10364=CARTESIAN_POINT('Ctrl Pts',(-24.740839166715,20.5554860564811,-66.4454875741169));
#10365=CARTESIAN_POINT('Ctrl Pts',(-24.7370405158981,20.5539789969895,-66.4452330711583));
#10366=CARTESIAN_POINT('Ctrl Pts',(-24.7353637942921,20.5533154103111,-66.4451208565448));
#10367=CARTESIAN_POINT('Ctrl Pts',(-24.7319650146108,20.5519735927565,-66.4448936432375));
#10368=CARTESIAN_POINT('Ctrl Pts',(-24.7302429313415,20.5512954388438,-66.444778649588));
#10369=CARTESIAN_POINT('Ctrl Pts',(-24.7267896123728,20.5499389618272,-66.444548312224));
#10370=CARTESIAN_POINT('Ctrl Pts',(-24.7250583805269,20.5492606561086,-66.4444329697345));
#10371=CARTESIAN_POINT('Ctrl Pts',(-24.7201905130804,20.5473582579889,-66.444109016382));
#10372=CARTESIAN_POINT('Ctrl Pts',(-24.717052533025,20.5461375777547,-66.4439006126907));
#10373=CARTESIAN_POINT('Ctrl Pts',(-24.7041802346993,20.5411534407962,-66.4430474466909));
#10374=CARTESIAN_POINT('Ctrl Pts',(-24.6944294351111,20.5374323074917,-66.4424052139725));
#10375=CARTESIAN_POINT('Ctrl Pts',(-24.5158515734184,20.4702748182372,-66.4307140261803));
#10376=CARTESIAN_POINT('Ctrl Pts',(-24.3419828773798,20.4210628707826,-66.4204768713474));
#10377=CARTESIAN_POINT('Ctrl Pts',(-24.0127956027335,20.3571073847874,-66.4016676881555));
#10378=CARTESIAN_POINT('Ctrl Pts',(-23.8587762695352,20.3385654020417,-66.3930873236593));
#10379=CARTESIAN_POINT('Ctrl Pts',(-23.6791967553484,20.3299872250672,-66.382873880477));
#10380=CARTESIAN_POINT('Ctrl Pts',(-23.6543590213605,20.3290886014673,-66.3814569341318));
#10381=CARTESIAN_POINT('Ctrl Pts',(-23.5299430702583,20.3260277570807,-66.3743311665365));
#10382=CARTESIAN_POINT('Ctrl Pts',(-23.4303203272242,20.3281955091975,-66.3685331090287));
#10383=CARTESIAN_POINT('Ctrl Pts',(-23.2839594681288,20.3381776172323,-66.3597834008424));
#10384=CARTESIAN_POINT('Ctrl Pts',(-23.2370330573755,20.3424136242046,-66.3569432147358));
#10385=CARTESIAN_POINT('Ctrl Pts',(-23.1824176809717,20.3485534981174,-66.3535916535463));
#10386=CARTESIAN_POINT('Ctrl Pts',(-23.1746204850187,20.3494589202903,-66.3531120719566));
#10387=CARTESIAN_POINT('Ctrl Pts',(-23.1627493133096,20.3508813931315,-66.3523802199701));
#10388=CARTESIAN_POINT('Ctrl Pts',(-23.1586728505169,20.3513777639725,-66.352128603742));
#10389=CARTESIAN_POINT('Ctrl Pts',(-23.15159552604,20.3522532660188,-66.3516912293978));
#10390=CARTESIAN_POINT('Ctrl Pts',(-23.1485942219393,20.3526288337707,-66.3515055842478));
#10391=CARTESIAN_POINT('Ctrl Pts',(-23.1423491713852,20.3534192383938,-66.351118949559));
#10392=CARTESIAN_POINT('Ctrl Pts',(-23.1391055200145,20.3538347881633,-66.3509179376462));
#10393=CARTESIAN_POINT('Ctrl Pts',(-23.1311880692332,20.3548613574252,-66.3504268060882));
#10394=CARTESIAN_POINT('Ctrl Pts',(-23.1265149769655,20.3554776938319,-66.3501365182975));
#10395=CARTESIAN_POINT('Ctrl Pts',(-23.1087437947588,20.3578612209542,-66.3490310232826));
#10396=CARTESIAN_POINT('Ctrl Pts',(-23.095655408496,20.3596987094098,-66.3482135911825));
#10397=CARTESIAN_POINT('Ctrl Pts',(-23.0781775686289,20.362262164749,-66.3471175997147));
#10398=CARTESIAN_POINT('Ctrl Pts',(-23.0737776463472,20.3629168051347,-66.3468413169962));
#10399=CARTESIAN_POINT('Ctrl Pts',(-22.8077250584586,20.403064526239,-66.3301123794968));
#10400=CARTESIAN_POINT('Ctrl Pts',(-22.5519883997415,20.4746146394046,-66.3125690605697));
#10401=CARTESIAN_POINT('Ctrl Pts',(-22.1545878240723,20.6406383934355,-66.2834382967805));
#10402=CARTESIAN_POINT('Ctrl Pts',(-22.0064253966681,20.7164674310688,-66.2721368524191));
#10403=CARTESIAN_POINT('Ctrl Pts',(-21.8230355555805,20.8289961560531,-66.258038586554));
#10404=CARTESIAN_POINT('Ctrl Pts',(-21.7818907212416,20.8555518378362,-66.2548690527379));
#10405=CARTESIAN_POINT('Ctrl Pts',(-21.7219335953938,20.8962143526388,-66.2502585419626));
#10406=CARTESIAN_POINT('Ctrl Pts',(-21.7026464225244,20.9096047830807,-66.2487767274542));
#10407=CARTESIAN_POINT('Ctrl Pts',(-21.680071821555,20.9256460032597,-66.24704554672));
#10408=CARTESIAN_POINT('Ctrl Pts',(-21.676641769872,20.9280934916388,-66.2467825942319));
#10409=CARTESIAN_POINT('Ctrl Pts',(-21.6713706534647,20.9318702818103,-66.2463786517707));
#10410=CARTESIAN_POINT('Ctrl Pts',(-21.6695261933851,20.9331948022367,-66.2462373329917));
#10411=CARTESIAN_POINT('Ctrl Pts',(-21.6663171806874,20.9355043625586,-66.2459915161325));
#10412=CARTESIAN_POINT('Ctrl Pts',(-21.6649520034552,20.936488519195,-66.2458869570627));
#10413=CARTESIAN_POINT('Ctrl Pts',(-21.662086573457,20.9385576213973,-66.2456675278944));
#10414=CARTESIAN_POINT('Ctrl Pts',(-21.6605864890141,20.939642787305,-66.2455526739214));
#10415=CARTESIAN_POINT('Ctrl Pts',(-21.656392827625,20.9426820038979,-66.2452316386186));
#10416=CARTESIAN_POINT('Ctrl Pts',(-21.6537013309078,20.9446389419303,-66.2450256583456));
#10417=CARTESIAN_POINT('Ctrl Pts',(-21.6428244343126,20.9525731166164,-66.2441934731213));
#10418=CARTESIAN_POINT('Ctrl Pts',(-21.6346641070276,20.958584867049,-66.2435696447985));
#10419=CARTESIAN_POINT('Ctrl Pts',(-21.4963063532975,21.0615241606773,-66.2329988990883));
#10420=CARTESIAN_POINT('Ctrl Pts',(-21.3735656624489,21.1681286920354,-66.2237104419028));
#10421=CARTESIAN_POINT('Ctrl Pts',(-21.0992543793937,21.4453658795981,-66.2017562007693));
#10422=CARTESIAN_POINT('Ctrl Pts',(-20.9567445012981,21.6236873340018,-66.1892583239405));
#10423=CARTESIAN_POINT('Ctrl Pts',(-20.7991668063294,21.8704061444507,-66.1723166568256));
#10424=CARTESIAN_POINT('Ctrl Pts',(-20.7657938792965,21.9263234180558,-66.1685018631107));
#10425=CARTESIAN_POINT('Ctrl Pts',(-20.7090689018598,22.0282632450615,-66.1615603765381));
#10426=CARTESIAN_POINT('Ctrl Pts',(-20.6850849961981,22.0739089617636,-66.1584567733095));
#10427=CARTESIAN_POINT('Ctrl Pts',(-20.6585312498045,22.1275318245967,-66.1548089848591));
#10428=CARTESIAN_POINT('Ctrl Pts',(-20.6548838856454,22.1349693148091,-66.1543030018873));
#10429=CARTESIAN_POINT('Ctrl Pts',(-20.6494318253231,22.1461961200596,-66.1535391441968));
#10430=CARTESIAN_POINT('Ctrl Pts',(-20.6476057709668,22.1499750735673,-66.1532820149934));
#10431=CARTESIAN_POINT('Ctrl Pts',(-20.6444714390372,22.1564939361144,-66.1528384274493));
#10432=CARTESIAN_POINT('Ctrl Pts',(-20.6431596387454,22.1592321533896,-66.1526520920368));
#10433=CARTESIAN_POINT('Ctrl Pts',(-20.6404600236735,22.1648877566394,-66.1522672092819));
#10434=CARTESIAN_POINT('Ctrl Pts',(-20.6390727226082,22.1678053830705,-66.1520686443257));
#10435=CARTESIAN_POINT('Ctrl Pts',(-20.6357336102024,22.1748551697919,-66.1515888285306));
#10436=CARTESIAN_POINT('Ctrl Pts',(-20.633786200317,22.178989397037,-66.1513074252707));
#10437=CARTESIAN_POINT('Ctrl Pts',(-20.626637096128,22.1942506087418,-66.1502685478638));
#10438=CARTESIAN_POINT('Ctrl Pts',(-20.6214902841984,22.2054030527326,-66.1495091767296));
#10439=CARTESIAN_POINT('Ctrl Pts',(-20.5393810004906,22.3860296555652,-66.1372064211835));
#10440=CARTESIAN_POINT('Ctrl Pts',(-20.4771926693296,22.5617974894936,-66.1251478992167));
#10441=CARTESIAN_POINT('Ctrl Pts',(-20.3952509043306,22.8780492991186,-66.103358340398));
#10442=CARTESIAN_POINT('Ctrl Pts',(-20.3689286290004,23.0163353492703,-66.0938095313974));
#10443=CARTESIAN_POINT('Ctrl Pts',(-20.3386688434436,23.2617618703957,-66.0770958621618));
#10444=CARTESIAN_POINT('Ctrl Pts',(-20.3308792220191,23.368222552258,-66.0699243602965));
#10445=CARTESIAN_POINT('Ctrl Pts',(-20.3271925380916,23.525811506521,-66.0595813255431));
#10446=CARTESIAN_POINT('Ctrl Pts',(-20.327208838471,23.5767681946769,-66.0562793311494));
#10447=CARTESIAN_POINT('Ctrl Pts',(-20.3288190679311,23.6437485863689,-66.0520127188152));
#10448=CARTESIAN_POINT('Ctrl Pts',(-20.3293245606241,23.6597883855573,-66.0509965633325));
#10449=CARTESIAN_POINT('Ctrl Pts',(-20.3303461945029,23.6859883444558,-66.0493465705868));
#10450=CARTESIAN_POINT('Ctrl Pts',(-20.3307906617731,23.6961508041276,-66.048708988274));
#10451=CARTESIAN_POINT('Ctrl Pts',(-20.3314383767592,23.70951100598,-66.0478741142288));
#10452=CARTESIAN_POINT('Ctrl Pts',(-20.3315982807305,23.712710645089,-66.0476744213109));
#10453=CARTESIAN_POINT('Ctrl Pts',(-20.3318680094599,23.7179510898089,-66.0473477771433));
#10454=CARTESIAN_POINT('Ctrl Pts',(-20.3319750044374,23.7199920290454,-66.0472206663492));
#10455=CARTESIAN_POINT('Ctrl Pts',(-20.3321846289019,23.7239191773237,-66.0469762829433));
#10456=CARTESIAN_POINT('Ctrl Pts',(-20.3322869750421,23.7258053926814,-66.0468589949062));
#10457=CARTESIAN_POINT('Ctrl Pts',(-20.3325268216191,23.7301550177445,-66.0465887329923));
#10458=CARTESIAN_POINT('Ctrl Pts',(-20.3326654929226,23.7326183667406,-66.0464358255604));
#10459=CARTESIAN_POINT('Ctrl Pts',(-20.3331060860646,23.740288073287,-66.0459602093124));
#10460=CARTESIAN_POINT('Ctrl Pts',(-20.333417818543,23.7454938922348,-66.0456380522005));
#10461=CARTESIAN_POINT('Ctrl Pts',(-20.3361580519968,23.7894656839561,-66.0429223695984));
#10462=CARTESIAN_POINT('Ctrl Pts',(-20.339274699465,23.8281876823985,-66.040566829082));
#10463=CARTESIAN_POINT('Ctrl Pts',(-20.3509521209117,23.9464825570983,-66.0334549623437));
#10464=CARTESIAN_POINT('Ctrl Pts',(-20.3617774855371,24.0258050545676,-66.0288028831895));
#10465=CARTESIAN_POINT('Ctrl Pts',(-20.376597460673,24.1106706183992,-66.0238746054057));
#10466=CARTESIAN_POINT('Ctrl Pts',(-20.3776663405971,24.1166903503323,-66.0235252986384));
#10467=CARTESIAN_POINT('Ctrl Pts',(-20.4168161095592,24.3335870648009,-66.0109480129169));
#10468=CARTESIAN_POINT('Ctrl Pts',(-20.4758177940231,24.5401487425338,-65.999225405155));
#10469=CARTESIAN_POINT('Ctrl Pts',(-20.5839751111098,24.8126037914481,-65.9825878293227));
#10470=CARTESIAN_POINT('Ctrl Pts',(-20.6157395292472,24.8847804459965,-65.9780642828652));
#10471=CARTESIAN_POINT('Ctrl Pts',(-20.6902557313299,25.0385425272825,-65.9680903897113));
#10472=CARTESIAN_POINT('Ctrl Pts',(-20.7339210691164,25.119603807354,-65.9626159874945));
#10473=CARTESIAN_POINT('Ctrl Pts',(-20.7862491274754,25.2075118283918,-65.9563889441812));
#10474=CARTESIAN_POINT('Ctrl Pts',(-20.7915483464408,25.2163180794572,-65.955761829817));
#10475=CARTESIAN_POINT('Ctrl Pts',(-20.79929975123,25.2290609992165,-65.9548494941112));
#10476=CARTESIAN_POINT('Ctrl Pts',(-20.8017184910905,25.2330180228588,-65.9545655021346));
#10477=CARTESIAN_POINT('Ctrl Pts',(-20.8059330822063,25.239879704705,-65.9540718454801));
#10478=CARTESIAN_POINT('Ctrl Pts',(-20.8077250290423,25.2427867622688,-65.9538623249818));
#10479=CARTESIAN_POINT('Ctrl Pts',(-20.8111808851454,25.2483732652159,-65.9534589637519));
#10480=CARTESIAN_POINT('Ctrl Pts',(-20.8128441148118,25.2510531283566,-65.9532651482984));
#10481=CARTESIAN_POINT('Ctrl Pts',(-20.8167737117797,25.2573639586262,-65.9528079693355));
#10482=CARTESIAN_POINT('Ctrl Pts',(-20.8190433800895,25.2609928547121,-65.9525444837134));
#10483=CARTESIAN_POINT('Ctrl Pts',(-20.8257739466888,25.2717065964667,-65.9517648146901));
#10484=CARTESIAN_POINT('Ctrl Pts',(-20.8302552056885,25.2787785516528,-65.9512478755268));
#10485=CARTESIAN_POINT('Ctrl Pts',(-20.870072421047,25.3410765560734,-65.9466736298149));
#10486=CARTESIAN_POINT('Ctrl Pts',(-20.9070561832937,25.395226286189,-65.942554861094));
#10487=CARTESIAN_POINT('Ctrl Pts',(-20.9604878088709,25.4685512238273,-65.9367697573062));
#10488=CARTESIAN_POINT('Ctrl Pts',(-20.9755497043263,25.4887200931725,-65.9351559316431));
#10489=CARTESIAN_POINT('Ctrl Pts',(-21.0411390212128,25.5744353703378,-65.9281996764234));
#10490=CARTESIAN_POINT('Ctrl Pts',(-21.0939415722647,25.6381944589174,-65.9227756631486));
#10491=CARTESIAN_POINT('Ctrl Pts',(-21.2836306839833,25.8500789202452,-65.9038972433279));
#10492=CARTESIAN_POINT('Ctrl Pts',(-21.4319252662477,25.9873526558733,-65.8901091452807));
#10493=CARTESIAN_POINT('Ctrl Pts',(-21.6534421512529,26.1568214640361,-65.8713947368684));
#10494=CARTESIAN_POINT('Ctrl Pts',(-21.7165013708092,26.20156341534,-65.8662574186317));
#10495=CARTESIAN_POINT('Ctrl Pts',(-21.8258949496183,26.2734086115919,-65.8577322747955));
#10496=CARTESIAN_POINT('Ctrl Pts',(-21.8714075916385,26.3017009857231,-65.8542927731693));
#10497=CARTESIAN_POINT('Ctrl Pts',(-21.9230549128523,26.3320478851358,-65.8505258811924));
#10498=CARTESIAN_POINT('Ctrl Pts',(-21.9285115990882,26.3352325726073,-65.8501295683718));
#10499=CARTESIAN_POINT('Ctrl Pts',(-21.938180106578,26.3408373546107,-65.8494303534324));
#10500=CARTESIAN_POINT('Ctrl Pts',(-21.9423880793123,26.3432639998438,-65.8491270378504));
#10501=CARTESIAN_POINT('Ctrl Pts',(-21.9486638510636,26.3468642160915,-65.8486761791317));
#10502=CARTESIAN_POINT('Ctrl Pts',(-21.9507274635199,26.3480450135629,-65.8485281687665));
#10503=CARTESIAN_POINT('Ctrl Pts',(-21.9542719978574,26.3500679899822,-65.8482743584731));
#10504=CARTESIAN_POINT('Ctrl Pts',(-21.9557522812448,26.3509112785297,-65.848168486018));
#10505=CARTESIAN_POINT('Ctrl Pts',(-21.9587848209065,26.3526356735627,-65.8479518498738));
#10506=CARTESIAN_POINT('Ctrl Pts',(-21.9603371373238,26.3535166625052,-65.8478410939265));
#10507=CARTESIAN_POINT('Ctrl Pts',(-21.9640619537037,26.3556265250596,-65.8475756595906));
#10508=CARTESIAN_POINT('Ctrl Pts',(-21.9662351549828,26.3568541676111,-65.8474210614054));
#10509=CARTESIAN_POINT('Ctrl Pts',(-21.974094335219,26.3612817866544,-65.8468629256106));
#10510=CARTESIAN_POINT('Ctrl Pts',(-21.979788652505,26.3644670470569,-65.846460334859));
#10511=CARTESIAN_POINT('Ctrl Pts',(-22.0150892582465,26.3840728234639,-65.8439754576728));
#10512=CARTESIAN_POINT('Ctrl Pts',(-22.0449407953315,26.4000419887913,-65.8419214485363));
#10513=CARTESIAN_POINT('Ctrl Pts',(-22.0750360187516,26.4155367763096,-65.8398919625532));
#10514=CARTESIAN_POINT('Origin',(-23.5502525316942,23.5502525316942,-77.3107734492734));
#10515=CARTESIAN_POINT('',(-22.0750359910842,26.4155367620648,-64.3441594845823));
#10516=CARTESIAN_POINT('',(-22.0750364910777,26.4155370194908,-64.5943742034087));
#10517=CARTESIAN_POINT('',(-22.0750360153461,26.4155367745563,-77.3107734492734));
#10518=CARTESIAN_POINT('Ctrl Pts',(-22.0750359910842,26.4155367620648,-64.3441594845823));
#10519=CARTESIAN_POINT('Ctrl Pts',(-22.0084775746858,26.3812685817053,-64.3484810791895));
#10520=CARTESIAN_POINT('Ctrl Pts',(-21.9431278129034,26.3446888022705,-64.3528636214976));
#10521=CARTESIAN_POINT('Ctrl Pts',(-21.8515820913567,26.2891706466032,-64.3592437283574));
#10522=CARTESIAN_POINT('Ctrl Pts',(-21.8243111707936,26.2720681043922,-64.3611759736847));
#10523=CARTESIAN_POINT('Ctrl Pts',(-21.7861117718246,26.2473069932409,-64.3639298983731));
#10524=CARTESIAN_POINT('Ctrl Pts',(-21.7749670867899,26.2399842971329,-64.3647391556141));
#10525=CARTESIAN_POINT('Ctrl Pts',(-21.7555470637995,26.2270509552216,-64.3661596662074));
#10526=CARTESIAN_POINT('Ctrl Pts',(-21.7472517372968,26.2214705401223,-64.3667697805453));
#10527=CARTESIAN_POINT('Ctrl Pts',(-21.7352452175298,26.2133121309472,-64.3676577640849));
#10528=CARTESIAN_POINT('Ctrl Pts',(-21.7315132110083,26.2107647498029,-64.3679344709718));
#10529=CARTESIAN_POINT('Ctrl Pts',(-21.7249740185168,26.2062810596693,-64.3684205385899));
#10530=CARTESIAN_POINT('Ctrl Pts',(-21.7221645192869,26.2043481235735,-64.3686297706183));
#10531=CARTESIAN_POINT('Ctrl Pts',(-21.7167573910592,26.2006153594685,-64.3690332259458));
#10532=CARTESIAN_POINT('Ctrl Pts',(-21.7141593296882,26.1988161618546,-64.3692274250124));
#10533=CARTESIAN_POINT('Ctrl Pts',(-21.7080284530673,26.1945570789215,-64.3696865084634));
#10534=CARTESIAN_POINT('Ctrl Pts',(-21.704497917967,26.1920939349554,-64.3699515174799));
#10535=CARTESIAN_POINT('Ctrl Pts',(-21.6922246468617,26.1834946454349,-64.3708750150888));
#10536=CARTESIAN_POINT('Ctrl Pts',(-21.6835075622683,26.1773221663067,-64.37153489844));
#10537=CARTESIAN_POINT('Ctrl Pts',(-21.5768025895898,26.1009662047092,-64.3796618097773));
#10538=CARTESIAN_POINT('Ctrl Pts',(-21.4828077900383,26.025391102516,-64.3873395839952));
#10539=CARTESIAN_POINT('Ctrl Pts',(-21.2498789545496,25.815566319872,-64.4078021367379));
#10540=CARTESIAN_POINT('Ctrl Pts',(-21.1183904879827,25.6737866426231,-64.4208607883527));
#10541=CARTESIAN_POINT('Ctrl Pts',(-20.8887423269359,25.3766725275494,-64.446270166219));
#10542=CARTESIAN_POINT('Ctrl Pts',(-20.7895581058479,25.222983601362,-64.4585674495632));
#10543=CARTESIAN_POINT('Ctrl Pts',(-20.6964671288916,25.0476765591401,-64.4711222455995));
#10544=CARTESIAN_POINT('Ctrl Pts',(-20.6891215500973,25.0335931446805,-64.4721209451804));
#10545=CARTESIAN_POINT('Ctrl Pts',(-20.6801699156034,25.0161165819596,-64.4733475352088));
#10546=CARTESIAN_POINT('Ctrl Pts',(-20.6784654364786,25.0127745032014,-64.4735815263109));
#10547=CARTESIAN_POINT('Ctrl Pts',(-20.6757926564775,25.007511128204,-64.4739491256729));
#10548=CARTESIAN_POINT('Ctrl Pts',(-20.6748204438805,25.0055918391305,-64.4740829809821));
#10549=CARTESIAN_POINT('Ctrl Pts',(-20.673008384112,25.0020056655004,-64.4743327321288));
#10550=CARTESIAN_POINT('Ctrl Pts',(-20.6721680686603,25.0003390360046,-64.4744486571299));
#10551=CARTESIAN_POINT('Ctrl Pts',(-20.6702867582708,24.9965996844143,-64.4747084321549));
#10552=CARTESIAN_POINT('Ctrl Pts',(-20.6692465550754,24.9945265725363,-64.4748522315438));
#10553=CARTESIAN_POINT('Ctrl Pts',(-20.6666120101656,24.9892617859158,-64.4752168623901));
#10554=CARTESIAN_POINT('Ctrl Pts',(-20.6650207239631,24.9860685739065,-64.475437501277));
#10555=CARTESIAN_POINT('Ctrl Pts',(-20.6563303676989,24.9685569713673,-64.4766446868571));
#10556=CARTESIAN_POINT('Ctrl Pts',(-20.6493324135397,24.954188238129,-64.4776249696025));
#10557=CARTESIAN_POINT('Ctrl Pts',(-20.5098795455314,24.6623579628047,-64.4973399133489));
#10558=CARTESIAN_POINT('Ctrl Pts',(-20.4176714462195,24.3673543489121,-64.5138332240417));
#10559=CARTESIAN_POINT('Ctrl Pts',(-20.3469327428879,23.9290283165571,-64.5389124052299));
#10560=CARTESIAN_POINT('Ctrl Pts',(-20.3337731321219,23.7931171707693,-64.5467450929553));
#10561=CARTESIAN_POINT('Ctrl Pts',(-20.3280383951876,23.6197368363614,-64.5570465088034));
#10562=CARTESIAN_POINT('Ctrl Pts',(-20.3274523232119,23.5826663728547,-64.5592663933931));
#10563=CARTESIAN_POINT('Ctrl Pts',(-20.3275273054129,23.5307812835165,-64.5624010924372));
#10564=CARTESIAN_POINT('Ctrl Pts',(-20.3276508546704,23.5159679355008,-64.5632992090104));
#10565=CARTESIAN_POINT('Ctrl Pts',(-20.3280423601303,23.4902719908224,-64.5648628157977));
#10566=CARTESIAN_POINT('Ctrl Pts',(-20.3282633342853,23.4793888440484,-64.5655268300316));
#10567=CARTESIAN_POINT('Ctrl Pts',(-20.3286581482601,23.4638286129281,-64.5664788064188));
#10568=CARTESIAN_POINT('Ctrl Pts',(-20.3287870479838,23.4591503802086,-64.5667653570792));
#10569=CARTESIAN_POINT('Ctrl Pts',(-20.3290283686361,23.4510341551103,-64.5672630801536));
#10570=CARTESIAN_POINT('Ctrl Pts',(-20.3291361047578,23.4475960224315,-64.5674741051214));
#10571=CARTESIAN_POINT('Ctrl Pts',(-20.3293522008616,23.441035394379,-64.567877134347));
#10572=CARTESIAN_POINT('Ctrl Pts',(-20.3294595975921,23.4379128692212,-64.5680691081167));
#10573=CARTESIAN_POINT('Ctrl Pts',(-20.3297206372422,23.4306314665606,-64.568517128443));
#10574=CARTESIAN_POINT('Ctrl Pts',(-20.3298777953998,23.4264727272431,-64.5687732852181));
#10575=CARTESIAN_POINT('Ctrl Pts',(-20.3304598049535,23.4118235253342,-64.5696765661007));
#10576=CARTESIAN_POINT('Ctrl Pts',(-20.3309278606915,23.4013349321328,-64.5703250463653));
#10577=CARTESIAN_POINT('Ctrl Pts',(-20.3365452090676,23.2879049411231,-64.5773573359795));
#10578=CARTESIAN_POINT('Ctrl Pts',(-20.3465782443687,23.1852756028663,-64.5838943922424));
#10579=CARTESIAN_POINT('Ctrl Pts',(-20.4060154570113,22.7793781670115,-64.6104853455971));
#10580=CARTESIAN_POINT('Ctrl Pts',(-20.4937502045334,22.4833821449497,-64.6317241747065));
#10581=CARTESIAN_POINT('Ctrl Pts',(-20.6518914266499,22.1393149607181,-64.6568511046693));
#10582=CARTESIAN_POINT('Ctrl Pts',(-20.6839480802668,22.0752805648507,-64.6615372176698));
#10583=CARTESIAN_POINT('Ctrl Pts',(-20.7323073995062,21.9862232721645,-64.6680164563072));
#10584=CARTESIAN_POINT('Ctrl Pts',(-20.7468632105,21.9602805940074,-64.6698990991851));
#10585=CARTESIAN_POINT('Ctrl Pts',(-20.7640311246103,21.9306513298193,-64.6720404667309));
#10586=CARTESIAN_POINT('Ctrl Pts',(-20.7662936582714,21.9267653053561,-64.6723211412749));
#10587=CARTESIAN_POINT('Ctrl Pts',(-20.7697318467019,21.9208883524733,-64.6727453314218));
#10588=CARTESIAN_POINT('Ctrl Pts',(-20.7709015108361,21.9188939533509,-64.6728892349461));
#10589=CARTESIAN_POINT('Ctrl Pts',(-20.7729284809082,21.9154462659832,-64.6731379109511));
#10590=CARTESIAN_POINT('Ctrl Pts',(-20.7737847804196,21.9139923947776,-64.6732427491346));
#10591=CARTESIAN_POINT('Ctrl Pts',(-20.7755722933839,21.9109629028236,-64.6734611477751));
#10592=CARTESIAN_POINT('Ctrl Pts',(-20.776503704683,21.9093874071681,-64.6735746945929));
#10593=CARTESIAN_POINT('Ctrl Pts',(-20.7790788108016,21.9050400359595,-64.6738879260228));
#10594=CARTESIAN_POINT('Ctrl Pts',(-20.7807253276463,21.9022698213049,-64.6740874255486));
#10595=CARTESIAN_POINT('Ctrl Pts',(-20.78717294842,21.8914588486191,-64.6748656288738));
#10596=CARTESIAN_POINT('Ctrl Pts',(-20.7920049981257,21.8834364604938,-64.6754423260525));
#10597=CARTESIAN_POINT('Ctrl Pts',(-20.8789081821557,21.7405686269903,-64.6857007361399));
#10598=CARTESIAN_POINT('Ctrl Pts',(-20.9707556639953,21.6118905156386,-64.6947565376803));
#10599=CARTESIAN_POINT('Ctrl Pts',(-21.1930141557245,21.3444457292551,-64.7143569741985));
#10600=CARTESIAN_POINT('Ctrl Pts',(-21.3270095794678,21.2094519330233,-64.7248084373697));
#10601=CARTESIAN_POINT('Ctrl Pts',(-21.5274882734812,21.0403138282139,-64.7397589892878));
#10602=CARTESIAN_POINT('Ctrl Pts',(-21.5844256504558,20.9954744038096,-64.7439350265669));
#10603=CARTESIAN_POINT('Ctrl Pts',(-21.7053186096723,20.9067041795223,-64.7527190482942));
#10604=CARTESIAN_POINT('Ctrl Pts',(-21.7694451687668,20.8630880947484,-64.7573339473016));
#10605=CARTESIAN_POINT('Ctrl Pts',(-21.8436777602657,20.8164231135643,-64.7626541752363));
#10606=CARTESIAN_POINT('Ctrl Pts',(-21.8523026932483,20.8110579273722,-64.7632719803187));
#10607=CARTESIAN_POINT('Ctrl Pts',(-21.8677795977599,20.8015316197536,-64.764380055032));
#10608=CARTESIAN_POINT('Ctrl Pts',(-21.8746220312211,20.7973551036713,-64.7648697547831));
#10609=CARTESIAN_POINT('Ctrl Pts',(-21.8850055717176,20.7910702055615,-64.7656126297876));
#10610=CARTESIAN_POINT('Ctrl Pts',(-21.8885352926462,20.7889429938562,-64.7658651140137));
#10611=CARTESIAN_POINT('Ctrl Pts',(-21.8946734647236,20.785259811889,-64.7663041101236));
#10612=CARTESIAN_POINT('Ctrl Pts',(-21.897280059026,20.7837007443487,-64.7664905083976));
#10613=CARTESIAN_POINT('Ctrl Pts',(-21.9026605916014,20.780492835461,-64.7668752265745));
#10614=CARTESIAN_POINT('Ctrl Pts',(-21.905434809492,20.7788444714209,-64.7670735636509));
#10615=CARTESIAN_POINT('Ctrl Pts',(-21.9129272587672,20.7744078766154,-64.7676091572903));
#10616=CARTESIAN_POINT('Ctrl Pts',(-21.9176501187945,20.7716275193373,-64.7679467002215));
#10617=CARTESIAN_POINT('Ctrl Pts',(-21.9350924264228,20.7614190194848,-64.7691930694488));
#10618=CARTESIAN_POINT('Ctrl Pts',(-21.9478555137149,20.7540661449043,-64.7701046225956));
#10619=CARTESIAN_POINT('Ctrl Pts',(-22.1677017608547,20.6294111904787,-64.785799947218));
#10620=CARTESIAN_POINT('Ctrl Pts',(-22.3870562334042,20.5353411152424,-64.8014488807902));
#10621=CARTESIAN_POINT('Ctrl Pts',(-22.7401388933511,20.4282320765578,-64.8263312982326));
#10622=CARTESIAN_POINT('Ctrl Pts',(-22.8677648278742,20.3978714285454,-64.8352487519946));
#10623=CARTESIAN_POINT('Ctrl Pts',(-23.1259038387993,20.3528790371021,-64.8528230810683));
#10624=CARTESIAN_POINT('Ctrl Pts',(-23.256191406017,20.338273989027,-64.8614630370889));
#10625=CARTESIAN_POINT('Ctrl Pts',(-23.3950345738884,20.3312325997467,-64.8701922570326));
#10626=CARTESIAN_POINT('Ctrl Pts',(-23.4030492212365,20.3308561402308,-64.8706944486077));
#10627=CARTESIAN_POINT('Ctrl Pts',(-23.4139876204163,20.3303832808681,-64.8713774465911));
#10628=CARTESIAN_POINT('Ctrl Pts',(-23.4169101330973,20.3302609286989,-64.8715596963508));
#10629=CARTESIAN_POINT('Ctrl Pts',(-23.421799257455,20.330062911183,-64.8718641907764));
#10630=CARTESIAN_POINT('Ctrl Pts',(-23.4237657716375,20.3299850683783,-64.8719865584346));
#10631=CARTESIAN_POINT('Ctrl Pts',(-23.4276380685225,20.3298353393001,-64.8722273028572));
#10632=CARTESIAN_POINT('Ctrl Pts',(-23.429543843673,20.3297633433386,-64.8723456856256));
#10633=CARTESIAN_POINT('Ctrl Pts',(-23.4337450111862,20.3296083669575,-64.8726064326707));
#10634=CARTESIAN_POINT('Ctrl Pts',(-23.4360404346669,20.3295261485382,-64.8727487537845));
#10635=CARTESIAN_POINT('Ctrl Pts',(-23.4440544510336,20.3292476774796,-64.8732451389146));
#10636=CARTESIAN_POINT('Ctrl Pts',(-23.4497735207077,20.3290641992999,-64.8735984856536));
#10637=CARTESIAN_POINT('Ctrl Pts',(-23.5073974232693,20.3273691344772,-64.877150021335));
#10638=CARTESIAN_POINT('Ctrl Pts',(-23.5593347415253,20.3270969005148,-64.8802800062925));
#10639=CARTESIAN_POINT('Ctrl Pts',(-23.6153102502501,20.3281567121641,-64.883598443716));
#10640=CARTESIAN_POINT('Ctrl Pts',(-23.6193608730062,20.3282410459234,-64.8838382695989));
#10641=CARTESIAN_POINT('Ctrl Pts',(-23.6386744084126,20.3286795904975,-64.8849803353228));
#10642=CARTESIAN_POINT('Ctrl Pts',(-23.6539350651345,20.3291346215477,-64.8858784725239));
#10643=CARTESIAN_POINT('Ctrl Pts',(-23.7236106389784,20.331707838893,-64.8899618954145));
#10644=CARTESIAN_POINT('Ctrl Pts',(-23.7779719198492,20.3350966444877,-64.8930999500953));
#10645=CARTESIAN_POINT('Ctrl Pts',(-24.0754586274404,20.3612251160705,-64.9101323130097));
#10646=CARTESIAN_POINT('Ctrl Pts',(-24.3154784023278,20.4101610528416,-64.9234219151308));
#10647=CARTESIAN_POINT('Ctrl Pts',(-24.6678242733373,20.5248408861135,-64.9446601460147));
#10648=CARTESIAN_POINT('Ctrl Pts',(-24.7855551141297,20.5709734163339,-64.9520593529787));
#10649=CARTESIAN_POINT('Ctrl Pts',(-24.9125952590026,20.6295806521088,-64.9605212875044));
#10650=CARTESIAN_POINT('Ctrl Pts',(-24.9248886397403,20.6353464446022,-64.9613451697864));
#10651=CARTESIAN_POINT('Ctrl Pts',(-24.9463086210551,20.6455583973451,-64.962789708507));
#10652=CARTESIAN_POINT('Ctrl Pts',(-24.9554513925886,20.6499703425965,-64.9634091756339));
#10653=CARTESIAN_POINT('Ctrl Pts',(-24.968655581336,20.6564192618527,-64.9643080690396));
#10654=CARTESIAN_POINT('Ctrl Pts',(-24.9727338403987,20.6584217740381,-64.9645862909656));
#10655=CARTESIAN_POINT('Ctrl Pts',(-24.9798697105791,20.6619443860795,-64.9650741432868));
#10656=CARTESIAN_POINT('Ctrl Pts',(-24.9829291728245,20.6634607373312,-64.9652836421277));
#10657=CARTESIAN_POINT('Ctrl Pts',(-24.9888100104368,20.6663870890744,-64.965686984105));
#10658=CARTESIAN_POINT('Ctrl Pts',(-24.9916317386184,20.6677963754775,-64.965880802002));
#10659=CARTESIAN_POINT('Ctrl Pts',(-24.9982783307557,20.6711281555412,-64.9663380210937));
#10660=CARTESIAN_POINT('Ctrl Pts',(-25.0021014355396,20.6730541290403,-64.9666015444737));
#10661=CARTESIAN_POINT('Ctrl Pts',(-25.0133927590193,20.6787706180989,-64.9673814271176));
#10662=CARTESIAN_POINT('Ctrl Pts',(-25.020850008822,20.6825826129165,-64.9678985427631));
#10663=CARTESIAN_POINT('Ctrl Pts',(-25.0866306501116,20.716532406551,-64.9724783304947));
#10664=CARTESIAN_POINT('Ctrl Pts',(-25.1440316224621,20.7484148034575,-64.9766026292053));
#10665=CARTESIAN_POINT('Ctrl Pts',(-25.2184300823927,20.7927643540135,-64.9821256712295));
#10666=CARTESIAN_POINT('Ctrl Pts',(-25.2363387576014,20.8036781931366,-64.9834690697035));
#10667=CARTESIAN_POINT('Ctrl Pts',(-25.3657100929598,20.8842613338654,-64.993275683542));
#10668=CARTESIAN_POINT('Ctrl Pts',(-25.4729128456745,20.9605100884085,-65.0019640912593));
#10669=CARTESIAN_POINT('Ctrl Pts',(-25.6479902492708,21.1019102060086,-65.017069013421));
#10670=CARTESIAN_POINT('Ctrl Pts',(-25.7182290019193,21.1638827065062,-65.0234113527737));
#10671=CARTESIAN_POINT('Ctrl Pts',(-25.9288228742058,21.366673677364,-65.0431971872683));
#10672=CARTESIAN_POINT('Ctrl Pts',(-26.0589397445547,21.5174900122687,-65.0565987601438));
#10673=CARTESIAN_POINT('Ctrl Pts',(-26.177921314709,21.6843714203939,-65.0694416680976));
#10674=CARTESIAN_POINT('Ctrl Pts',(-26.1814852000778,21.6894005222466,-65.0698269501758));
#10675=CARTESIAN_POINT('Ctrl Pts',(-26.1865493999315,21.6965903984527,-65.0703752433461));
#10676=CARTESIAN_POINT('Ctrl Pts',(-26.1880615028128,21.6987427926714,-65.070539061005));
#10677=CARTESIAN_POINT('Ctrl Pts',(-26.1906664955088,21.702460523155,-65.0708214571442));
#10678=CARTESIAN_POINT('Ctrl Pts',(-26.1917606311474,21.7040249813298,-65.0709401219274));
#10679=CARTESIAN_POINT('Ctrl Pts',(-26.1938609160099,21.7070337787279,-65.0711680119013));
#10680=CARTESIAN_POINT('Ctrl Pts',(-26.1948672701956,21.7084779673543,-65.0712772514315));
#10681=CARTESIAN_POINT('Ctrl Pts',(-26.1972444204015,21.7118953096053,-65.0715354007722));
#10682=CARTESIAN_POINT('Ctrl Pts',(-26.1986141964559,21.7138691764011,-65.0716842400786));
#10683=CARTESIAN_POINT('Ctrl Pts',(-26.2026809556031,21.719743448047,-65.0721263972778));
#10684=CARTESIAN_POINT('Ctrl Pts',(-26.2053715538687,21.7236482975918,-65.0724192792467));
#10685=CARTESIAN_POINT('Ctrl Pts',(-26.2297959281024,21.7592632427426,-65.075081280745));
#10686=CARTESIAN_POINT('Ctrl Pts',(-26.2509704725904,21.7913556129217,-65.0774130830908));
#10687=CARTESIAN_POINT('Ctrl Pts',(-26.4396209105045,22.0887187542884,-65.0984884994713));
#10688=CARTESIAN_POINT('Ctrl Pts',(-26.5681213071658,22.3767700032099,-65.1152300366911));
#10689=CARTESIAN_POINT('Ctrl Pts',(-26.6794214422486,22.7730835381143,-65.138680670615));
#10690=CARTESIAN_POINT('Ctrl Pts',(-26.7015696531645,22.8684257599818,-65.1443375690071));
#10691=CARTESIAN_POINT('Ctrl Pts',(-26.7308926452289,23.0271049178819,-65.1538864016768));
#10692=CARTESIAN_POINT('Ctrl Pts',(-26.7405880006278,23.0899116826497,-65.157699358001));
#10693=CARTESIAN_POINT('Ctrl Pts',(-26.7494553997721,23.1612935654842,-65.1620839835335));
#10694=CARTESIAN_POINT('Ctrl Pts',(-26.7504579544631,23.1696302537192,-65.1625968416013));
#10695=CARTESIAN_POINT('Ctrl Pts',(-26.751915400691,23.1821625360444,-65.1633690042969));
#10696=CARTESIAN_POINT('Ctrl Pts',(-26.7523946554713,23.1863553065399,-65.163627538691));
#10697=CARTESIAN_POINT('Ctrl Pts',(-26.7532049032219,23.1935693308576,-65.1640727202607));
#10698=CARTESIAN_POINT('Ctrl Pts',(-26.7535398609064,23.1965901412174,-65.164259241945));
#10699=CARTESIAN_POINT('Ctrl Pts',(-26.7542210321389,23.2028136338694,-65.1646437347373));
#10700=CARTESIAN_POINT('Ctrl Pts',(-26.7545667179524,23.2060163697634,-65.16484172231));
#10701=CARTESIAN_POINT('Ctrl Pts',(-26.7553876055673,23.213730175321,-65.1653188672145));
#10702=CARTESIAN_POINT('Ctrl Pts',(-26.7558580854776,23.2182417316635,-65.1655981733355));
#10703=CARTESIAN_POINT('Ctrl Pts',(-26.7572734846272,23.2320978769842,-65.1664567375372));
#10704=CARTESIAN_POINT('Ctrl Pts',(-26.7581870733668,23.2414455528069,-65.1670369829208));
#10705=CARTESIAN_POINT('Ctrl Pts',(-26.7684121882538,23.3510124847005,-65.1738506383671));
#10706=CARTESIAN_POINT('Ctrl Pts',(-26.7730637826178,23.4516008112041,-65.1802303852552));
#10707=CARTESIAN_POINT('Ctrl Pts',(-26.7729350406849,23.6610365978374,-65.1937925066299));
#10708=CARTESIAN_POINT('Ctrl Pts',(-26.7673583309661,23.7697571657355,-65.2009897763069));
#10709=CARTESIAN_POINT('Ctrl Pts',(-26.7270989511482,24.1636012495447,-65.2275235236627));
#10710=CARTESIAN_POINT('Ctrl Pts',(-26.659866716583,24.444042878652,-65.2474229664955));
#10711=CARTESIAN_POINT('Ctrl Pts',(-26.5507991379999,24.726295342832,-65.2665680271834));
#10712=CARTESIAN_POINT('Ctrl Pts',(-26.5451221681728,24.7406778815255,-65.2675406787582));
#10713=CARTESIAN_POINT('Ctrl Pts',(-26.537922087815,24.7585416560827,-65.2687446221201));
#10714=CARTESIAN_POINT('Ctrl Pts',(-26.5364961691152,24.7620614782761,-65.2689816425189));
#10715=CARTESIAN_POINT('Ctrl Pts',(-26.534162549184,24.7677927915935,-65.2693672446922));
#10716=CARTESIAN_POINT('Ctrl Pts',(-26.5332586089696,24.7700057936145,-65.2695160531767));
#10717=CARTESIAN_POINT('Ctrl Pts',(-26.5316420250063,24.7739509258093,-65.2697811858601));
#10718=CARTESIAN_POINT('Ctrl Pts',(-26.530930334254,24.7756834387575,-65.2698975679619));
#10719=CARTESIAN_POINT('Ctrl Pts',(-26.5294158455725,24.7793611273311,-65.2701445078536));
#10720=CARTESIAN_POINT('Ctrl Pts',(-26.5286126548516,24.781306132263,-65.2702750409053));
#10721=CARTESIAN_POINT('Ctrl Pts',(-26.5264531684644,24.7865210559381,-65.2706248534712));
#10722=CARTESIAN_POINT('Ctrl Pts',(-26.5250933841461,24.7897895409103,-65.2708439200457));
#10723=CARTESIAN_POINT('Ctrl Pts',(-26.51856952824,24.8053982276568,-65.2718892419742));
#10724=CARTESIAN_POINT('Ctrl Pts',(-26.5133339436695,24.8177086732732,-65.2727111883452));
#10725=CARTESIAN_POINT('Ctrl Pts',(-26.4701358269832,24.9175497899187,-65.2793598978412));
#10726=CARTESIAN_POINT('Ctrl Pts',(-26.4283760123026,25.0033971733467,-65.284967353444));
#10727=CARTESIAN_POINT('Ctrl Pts',(-26.195407156903,25.4327409028723,-65.3130707163497));
#10728=CARTESIAN_POINT('Ctrl Pts',(-25.9463529969348,25.7409944884951,-65.3339114055139));
#10729=CARTESIAN_POINT('Ctrl Pts',(-25.6333752698002,26.0093345444917,-65.3588609965977));
#10730=CARTESIAN_POINT('Ctrl Pts',(-25.6187185311786,26.0216758204029,-65.3600257966169));
#10731=CARTESIAN_POINT('Ctrl Pts',(-25.5992503583751,26.037773929074,-65.3615686288551));
#10732=CARTESIAN_POINT('Ctrl Pts',(-25.5945368512947,26.0416490107781,-65.3619418374649));
#10733=CARTESIAN_POINT('Ctrl Pts',(-25.5872176048275,26.0476315747174,-65.3625208637987));
#10734=CARTESIAN_POINT('Ctrl Pts',(-25.5846195179861,26.0497484326003,-65.3627263013991));
#10735=CARTESIAN_POINT('Ctrl Pts',(-25.5794211522793,26.0539704600855,-65.3631371581688));
#10736=CARTESIAN_POINT('Ctrl Pts',(-25.5768208876912,26.056075640785,-65.3633425765327));
#10737=CARTESIAN_POINT('Ctrl Pts',(-25.5710230100465,26.0607546898062,-65.3638003934027));
#10738=CARTESIAN_POINT('Ctrl Pts',(-25.5678237521995,26.0633265023534,-65.3640528742376));
#10739=CARTESIAN_POINT('Ctrl Pts',(-25.5584982857068,26.0707937533083,-65.3647884211801));
#10740=CARTESIAN_POINT('Ctrl Pts',(-25.5523591438132,26.0756729264667,-65.365272138872));
#10741=CARTESIAN_POINT('Ctrl Pts',(-25.5086157646266,26.110178865844,-65.3687152860815));
#10742=CARTESIAN_POINT('Ctrl Pts',(-25.47037500251,26.1389855590292,-65.3717071468882));
#10743=CARTESIAN_POINT('Ctrl Pts',(-25.3469472302823,26.2277237953631,-65.3813139794789));
#10744=CARTESIAN_POINT('Ctrl Pts',(-25.2594971712277,26.2843781960521,-65.3880499131564));
#10745=CARTESIAN_POINT('Ctrl Pts',(-25.0244234204579,26.4209804670512,-65.4059645346111));
#10746=CARTESIAN_POINT('Ctrl Pts',(-24.8730317143905,26.4938057603953,-65.4173281181204));
#10747=CARTESIAN_POINT('Ctrl Pts',(-24.542985623257,26.6219481622529,-65.4412827409213));
#10748=CARTESIAN_POINT('Ctrl Pts',(-24.3637519180212,26.6742035221455,-65.453825618138));
#10749=CARTESIAN_POINT('Ctrl Pts',(-24.1701065142083,26.7128498345631,-65.4662648202726));
#10750=CARTESIAN_POINT('Ctrl Pts',(-24.1592148256802,26.7149650925464,-65.4669607545297));
#10751=CARTESIAN_POINT('Ctrl Pts',(-24.144922231777,26.7176643161578,-65.4678689318156));
#10752=CARTESIAN_POINT('Ctrl Pts',(-24.1415311760027,26.7182990953681,-65.468084032759));
#10753=CARTESIAN_POINT('Ctrl Pts',(-24.1362945362004,26.7192706526495,-65.4684156200827));
#10754=CARTESIAN_POINT('Ctrl Pts',(-24.1344496797699,26.7196112640266,-65.4685323260258));
#10755=CARTESIAN_POINT('Ctrl Pts',(-24.1308053417288,26.7202808191979,-65.4687626458208));
#10756=CARTESIAN_POINT('Ctrl Pts',(-24.1290058881236,26.720609839832,-65.4688762632045));
#10757=CARTESIAN_POINT('Ctrl Pts',(-24.1252070837139,26.721301089216,-65.4691158944927));
#10758=CARTESIAN_POINT('Ctrl Pts',(-24.1232076765211,26.7216629581638,-65.4692418872324));
#10759=CARTESIAN_POINT('Ctrl Pts',(-24.1173152410103,26.7227236647679,-65.4696128161012));
#10760=CARTESIAN_POINT('Ctrl Pts',(-24.1134212487841,26.7234172300627,-65.4698574502076));
#10761=CARTESIAN_POINT('Ctrl Pts',(-24.1046992139936,26.7249541649067,-65.470404315691));
#10762=CARTESIAN_POINT('Ctrl Pts',(-24.0998704920695,26.7257936953081,-65.4707063307718));
#10763=CARTESIAN_POINT('Ctrl Pts',(-23.9168811976172,26.7571786581925,-65.4821240272049));
#10764=CARTESIAN_POINT('Ctrl Pts',(-23.7364364486107,26.7726970580989,-65.4924048748776));
#10765=CARTESIAN_POINT('Ctrl Pts',(-23.4809634182051,26.7731223422212,-65.506743911095));
#10766=CARTESIAN_POINT('Ctrl Pts',(-23.4063271725404,26.7706525756122,-65.510905695665));
#10767=CARTESIAN_POINT('Ctrl Pts',(-23.0879113990273,26.749023506195,-65.5287528544426));
#10768=CARTESIAN_POINT('Ctrl Pts',(-22.8466985244271,26.7047543808934,-65.5425816558037));
#10769=CARTESIAN_POINT('Ctrl Pts',(-22.597867796705,26.6291038221533,-65.5583548142092));
#10770=CARTESIAN_POINT('Ctrl Pts',(-22.5829442922181,26.6244478261717,-65.5593064272317));
#10771=CARTESIAN_POINT('Ctrl Pts',(-22.562705066674,26.6179714113744,-65.5606048596276));
#10772=CARTESIAN_POINT('Ctrl Pts',(-22.5573591899102,26.616245345062,-65.5609485683036));
#10773=CARTESIAN_POINT('Ctrl Pts',(-22.5489237998476,26.6134973672529,-65.5614921063162));
#10774=CARTESIAN_POINT('Ctrl Pts',(-22.5458312570651,26.6124847330051,-65.5616916290606));
#10775=CARTESIAN_POINT('Ctrl Pts',(-22.5398633786689,26.6105205746805,-65.5620771525766));
#10776=CARTESIAN_POINT('Ctrl Pts',(-22.536987838921,26.6095696773584,-65.5622631324607));
#10777=CARTESIAN_POINT('Ctrl Pts',(-22.5301840478873,26.6073091221488,-65.5627037027011));
#10778=CARTESIAN_POINT('Ctrl Pts',(-22.5262569788714,26.6059959463877,-65.5629584092901));
#10779=CARTESIAN_POINT('Ctrl Pts',(-22.5147376242487,26.6021192806462,-65.5637067694691));
#10780=CARTESIAN_POINT('Ctrl Pts',(-22.5071523974263,26.5995350513916,-65.5642011099872));
#10781=CARTESIAN_POINT('Ctrl Pts',(-22.4503080688531,26.5799316983751,-65.5679175901888));
#10782=CARTESIAN_POINT('Ctrl Pts',(-22.4014611003064,26.561749071201,-65.5711782838609));
#10783=CARTESIAN_POINT('Ctrl Pts',(-22.2584255701523,26.504519633226,-65.5809342208569));
#10784=CARTESIAN_POINT('Ctrl Pts',(-22.1656416631724,26.4621858811723,-65.5875364717936));
#10785=CARTESIAN_POINT('Ctrl Pts',(-22.0750359980476,26.41553676565,-65.5942565421953));
#10786=CARTESIAN_POINT('Ctrl Pts',(-22.0750360187516,26.4155367763096,-65.8398919625532));
#10787=CARTESIAN_POINT('Ctrl Pts',(-22.1314774174797,26.4445961213201,-65.8360858094642));
#10788=CARTESIAN_POINT('Ctrl Pts',(-22.1887759126829,26.471986968196,-65.8323658270479));
#10789=CARTESIAN_POINT('Ctrl Pts',(-22.512340525602,26.6150723552368,-65.8119484436766));
#10790=CARTESIAN_POINT('Ctrl Pts',(-22.7924736465595,26.6960712839078,-65.7963290618333));
#10791=CARTESIAN_POINT('Ctrl Pts',(-23.1612705816343,26.750504389791,-65.7748150913148));
#10792=CARTESIAN_POINT('Ctrl Pts',(-23.2432836255907,26.7594093343291,-65.769982713062));
#10793=CARTESIAN_POINT('Ctrl Pts',(-23.3679980260237,26.7681263728235,-65.7625092541809));
#10794=CARTESIAN_POINT('Ctrl Pts',(-23.4105056052571,26.770252422188,-65.7599403299434));
#10795=CARTESIAN_POINT('Ctrl Pts',(-23.4606764310766,26.7717664665596,-65.7568788778994));
#10796=CARTESIAN_POINT('Ctrl Pts',(-23.4683122732181,26.7719697295236,-65.756412134515));
#10797=CARTESIAN_POINT('Ctrl Pts',(-23.4800094694729,26.772239492129,-65.7556958905477));
#10798=CARTESIAN_POINT('Ctrl Pts',(-23.4840703831691,26.7723254644472,-65.75544700172));
#10799=CARTESIAN_POINT('Ctrl Pts',(-23.4914742764207,26.7724682069644,-65.7549928011584));
#10800=CARTESIAN_POINT('Ctrl Pts',(-23.4948172071824,26.7725274526021,-65.7547875674522));
#10801=CARTESIAN_POINT('Ctrl Pts',(-23.501536784661,26.7726360815994,-65.7543747107968));
#10802=CARTESIAN_POINT('Ctrl Pts',(-23.5049134286529,26.7726853599011,-65.7541670848094));
#10803=CARTESIAN_POINT('Ctrl Pts',(-23.5145185033408,26.7728104351126,-65.7535760154035));
#10804=CARTESIAN_POINT('Ctrl Pts',(-23.5207470597465,26.7728734817781,-65.7531921721055));
#10805=CARTESIAN_POINT('Ctrl Pts',(-23.5471574610716,26.7730642399325,-65.7515622104544));
#10806=CARTESIAN_POINT('Ctrl Pts',(-23.5673397404734,26.7730204233788,-65.7503107195909));
#10807=CARTESIAN_POINT('Ctrl Pts',(-23.5922482618142,26.7727323658301,-65.7487586128242));
#10808=CARTESIAN_POINT('Ctrl Pts',(-23.5969764628257,26.772667277911,-65.7484636524649));
#10809=CARTESIAN_POINT('Ctrl Pts',(-23.6133326716906,26.7724061139555,-65.7474421317708));
#10810=CARTESIAN_POINT('Ctrl Pts',(-23.6249596448422,26.772157504418,-65.7467139311696));
#10811=CARTESIAN_POINT('Ctrl Pts',(-23.6413024748774,26.7717195487347,-65.7456874630577));
#10812=CARTESIAN_POINT('Ctrl Pts',(-23.6460197500507,26.7715827652374,-65.7453908371267));
#10813=CARTESIAN_POINT('Ctrl Pts',(-23.6572498467769,26.7712324446381,-65.744683863835));
#10814=CARTESIAN_POINT('Ctrl Pts',(-23.6637623358899,26.7710095154437,-65.7442732265932));
#10815=CARTESIAN_POINT('Ctrl Pts',(-23.672156800396,26.7706966720861,-65.7437430760183));
#10816=CARTESIAN_POINT('Ctrl Pts',(-23.6740394698188,26.7706248558266,-65.7436241214735));
#10817=CARTESIAN_POINT('Ctrl Pts',(-23.6828619587963,26.7702805653793,-65.7430664235186));
#10818=CARTESIAN_POINT('Ctrl Pts',(-23.6898009081286,26.769987310725,-65.7426270419655));
#10819=CARTESIAN_POINT('Ctrl Pts',(-23.7016143350283,26.7694497898516,-65.7418777228726));
#10820=CARTESIAN_POINT('Ctrl Pts',(-23.7064893261831,26.7692168754028,-65.7415681334758));
#10821=CARTESIAN_POINT('Ctrl Pts',(-23.7153710777188,26.7687723043821,-65.7410034134315));
#10822=CARTESIAN_POINT('Ctrl Pts',(-23.719378014702,26.7685642369506,-65.7407483923209));
#10823=CARTESIAN_POINT('Ctrl Pts',(-23.99917912757,26.7535110732843,-65.7229228557281));
#10824=CARTESIAN_POINT('Ctrl Pts',(-24.2718791504951,26.7032826107241,-65.7042041508269));
#10825=CARTESIAN_POINT('Ctrl Pts',(-24.6986824843514,26.5663524062377,-65.673923930312));
#10826=CARTESIAN_POINT('Ctrl Pts',(-24.8581408151541,26.5007091863637,-65.6624080022885));
#10827=CARTESIAN_POINT('Ctrl Pts',(-25.0184237292761,26.4191633638485,-65.6511201129068));
#10828=CARTESIAN_POINT('Ctrl Pts',(-25.0252264501066,26.4156718676909,-65.6506416227527));
#10829=CARTESIAN_POINT('Ctrl Pts',(-25.0345590548929,26.4108398671108,-65.6499860649508));
#10830=CARTESIAN_POINT('Ctrl Pts',(-25.0370996043509,26.4095201898614,-65.649807696919));
#10831=CARTESIAN_POINT('Ctrl Pts',(-25.0413832355585,26.4072878233483,-65.6495071058993));
#10832=CARTESIAN_POINT('Ctrl Pts',(-25.0431272399276,26.4063769231259,-65.6493847693261));
#10833=CARTESIAN_POINT('Ctrl Pts',(-25.0465605481488,26.4045796891342,-65.6491440210579));
#10834=CARTESIAN_POINT('Ctrl Pts',(-25.0482498992065,26.4036934525414,-65.6490256034622));
#10835=CARTESIAN_POINT('Ctrl Pts',(-25.0519731796792,26.4017359951345,-65.6487647050373));
#10836=CARTESIAN_POINT('Ctrl Pts',(-25.0540067554474,26.4006640952197,-65.6486222675436));
#10837=CARTESIAN_POINT('Ctrl Pts',(-25.0611078771453,26.3969113722204,-65.648125086871));
#10838=CARTESIAN_POINT('Ctrl Pts',(-25.0661694539003,26.3942191832906,-65.6477710640184));
#10839=CARTESIAN_POINT('Ctrl Pts',(-25.1173343843339,26.3668297973865,-65.6441958033327));
#10840=CARTESIAN_POINT('Ctrl Pts',(-25.1628404717761,26.3410255311583,-65.6410437648488));
#10841=CARTESIAN_POINT('Ctrl Pts',(-25.2113263328911,26.3119493389905,-65.6376935661277));
#10842=CARTESIAN_POINT('Ctrl Pts',(-25.2149470381323,26.3097683640534,-65.6374434390298));
#10843=CARTESIAN_POINT('Ctrl Pts',(-25.2265368853065,26.3027559699556,-65.6366429122394));
#10844=CARTESIAN_POINT('Ctrl Pts',(-25.2344894276581,26.2978970672107,-65.6360938134113));
#10845=CARTESIAN_POINT('Ctrl Pts',(-25.3259209822222,26.2414874361403,-65.629781664611));
#10846=CARTESIAN_POINT('Ctrl Pts',(-25.4070311544467,26.1861811378678,-65.6241900169108));
#10847=CARTESIAN_POINT('Ctrl Pts',(-25.542601059139,26.0843726693974,-65.6146362363909));
#10848=CARTESIAN_POINT('Ctrl Pts',(-25.5982654136853,26.0396020560029,-65.6106478055526));
#10849=CARTESIAN_POINT('Ctrl Pts',(-25.7739224121444,25.888438828471,-65.5976990712599));
#10850=CARTESIAN_POINT('Ctrl Pts',(-25.8874689116535,25.7749407931563,-65.5887375817911));
#10851=CARTESIAN_POINT('Ctrl Pts',(-26.0432893493065,25.5940331251387,-65.57492121108));
#10852=CARTESIAN_POINT('Ctrl Pts',(-26.0922952639063,25.5327481847895,-65.5703135740271));
#10853=CARTESIAN_POINT('Ctrl Pts',(-26.1627246385627,25.4377619558782,-65.5632347871806));
#10854=CARTESIAN_POINT('Ctrl Pts',(-26.1858398109791,25.4053487049488,-65.5608298025226));
#10855=CARTESIAN_POINT('Ctrl Pts',(-26.2125647979794,25.3663655726633,-65.5579465997368));
#10856=CARTESIAN_POINT('Ctrl Pts',(-26.2167603078255,25.360199895334,-65.5574908568229));
#10857=CARTESIAN_POINT('Ctrl Pts',(-26.223186077618,25.3506858148184,-65.5567880088567));
#10858=CARTESIAN_POINT('Ctrl Pts',(-26.2254315512978,25.347347676851,-65.5565414802568));
#10859=CARTESIAN_POINT('Ctrl Pts',(-26.2295133194141,25.3412550869365,-65.5560916615716));
#10860=CARTESIAN_POINT('Ctrl Pts',(-26.2313516341703,25.3385019897034,-65.5558884481435));
#10861=CARTESIAN_POINT('Ctrl Pts',(-26.2350653345793,25.3329216782839,-65.5554766472879));
#10862=CARTESIAN_POINT('Ctrl Pts',(-26.2369405039706,25.3300943258498,-65.5552680520602));
#10863=CARTESIAN_POINT('Ctrl Pts',(-26.2422886511229,25.3220027589538,-65.5546712155981));
#10864=CARTESIAN_POINT('Ctrl Pts',(-26.2457506314776,25.3167313255839,-65.5542825618004));
#10865=CARTESIAN_POINT('Ctrl Pts',(-26.2605810346517,25.294004492594,-65.5526076444245));
#10866=CARTESIAN_POINT('Ctrl Pts',(-26.2717953401025,25.2764495668755,-65.5513156350807));
#10867=CARTESIAN_POINT('Ctrl Pts',(-26.4700106112287,24.9594292678118,-65.5280107266666));
#10868=CARTESIAN_POINT('Ctrl Pts',(-26.6066807566537,24.6313990096662,-65.5039308927914));
#10869=CARTESIAN_POINT('Ctrl Pts',(-26.7193997442931,24.1520093008839,-65.4708344970097));
#10870=CARTESIAN_POINT('Ctrl Pts',(-26.7424932825477,24.014164935585,-65.4615962731825));
#10871=CARTESIAN_POINT('Ctrl Pts',(-26.7573960492333,23.867134849688,-65.4523156917197));
#10872=CARTESIAN_POINT('Ctrl Pts',(-26.7581869347573,23.859025611195,-65.4518056819921));
#10873=CARTESIAN_POINT('Ctrl Pts',(-26.7592216258119,23.8479832429826,-65.4511137953029));
#10874=CARTESIAN_POINT('Ctrl Pts',(-26.7594921706662,23.8450527407568,-65.4509304260897));
#10875=CARTESIAN_POINT('Ctrl Pts',(-26.7599372923853,23.8401580129626,-65.4506245699247));
#10876=CARTESIAN_POINT('Ctrl Pts',(-26.7601140805964,23.8381939979885,-65.4505019576399));
#10877=CARTESIAN_POINT('Ctrl Pts',(-26.76045806278,23.8343328683161,-65.4502611330765));
#10878=CARTESIAN_POINT('Ctrl Pts',(-26.760625377734,23.8324357681029,-65.4501429141497));
#10879=CARTESIAN_POINT('Ctrl Pts',(-26.7609898518722,23.8282608956167,-65.4498829858334));
#10880=CARTESIAN_POINT('Ctrl Pts',(-26.7611862694014,23.8259830554392,-65.4497413185837));
#10881=CARTESIAN_POINT('Ctrl Pts',(-26.7618420034747,23.8182828292119,-65.4492629194358));
#10882=CARTESIAN_POINT('Ctrl Pts',(-26.7622900132213,23.8128594507389,-65.4489268244761));
#10883=CARTESIAN_POINT('Ctrl Pts',(-26.7663327098574,23.7623620235274,-65.445805102344));
#10884=CARTESIAN_POINT('Ctrl Pts',(-26.76899235934,23.7172153464584,-65.443071098864));
#10885=CARTESIAN_POINT('Ctrl Pts',(-26.7708284766172,23.6686565330669,-65.4401772796194));
#10886=CARTESIAN_POINT('Ctrl Pts',(-26.7709505576056,23.6652879637579,-65.4399767746132));
#10887=CARTESIAN_POINT('Ctrl Pts',(-26.7711697273477,23.6589664249128,-65.4396009456666));
#10888=CARTESIAN_POINT('Ctrl Pts',(-26.7712680405932,23.6560135046231,-65.4394255698778));
#10889=CARTESIAN_POINT('Ctrl Pts',(-26.7715691168757,23.6465803808073,-65.4388658990904));
#10890=CARTESIAN_POINT('Ctrl Pts',(-26.7717563871692,23.6400996622086,-65.43848225231));
#10891=CARTESIAN_POINT('Ctrl Pts',(-26.7726273147288,23.6064426820705,-65.4364940671712));
#10892=CARTESIAN_POINT('Ctrl Pts',(-26.7729866680792,23.5792584294255,-65.4349026124946));
#10893=CARTESIAN_POINT('Ctrl Pts',(-26.773048947276,23.4689556087308,-65.4284919347338));
#10894=CARTESIAN_POINT('Ctrl Pts',(-26.7698804175324,23.3858637622659,-65.4237700562543));
#10895=CARTESIAN_POINT('Ctrl Pts',(-26.744464316596,23.0555827727251,-65.4051213362025));
#10896=CARTESIAN_POINT('Ctrl Pts',(-26.6969206326827,22.8112240568182,-65.3915218427683));
#10897=CARTESIAN_POINT('Ctrl Pts',(-26.5934761572848,22.4855120939023,-65.3715850037452));
#10898=CARTESIAN_POINT('Ctrl Pts',(-26.561265720256,22.3975690477003,-65.3660184613766));
#10899=CARTESIAN_POINT('Ctrl Pts',(-26.5213357508337,22.3016985358388,-65.3596965290186));
#10900=CARTESIAN_POINT('Ctrl Pts',(-26.5173506599199,22.2922575916068,-65.3590712056871));
#10901=CARTESIAN_POINT('Ctrl Pts',(-26.5117000674537,22.2790471839711,-65.3581922731352));
#10902=CARTESIAN_POINT('Ctrl Pts',(-26.5100722309835,22.2752615942449,-65.3579399501656));
#10903=CARTESIAN_POINT('Ctrl Pts',(-26.5070776569435,22.2683342504457,-65.3574773798299));
#10904=CARTESIAN_POINT('Ctrl Pts',(-26.5057131592454,22.2651915292661,-65.357267209307));
#10905=CARTESIAN_POINT('Ctrl Pts',(-26.5029430097323,22.2588390495612,-65.356841741466));
#10906=CARTESIAN_POINT('Ctrl Pts',(-26.5015371297971,22.2556293966555,-65.3566264365744));
#10907=CARTESIAN_POINT('Ctrl Pts',(-26.4980727518136,22.247755119588,-65.3560974051145));
#10908=CARTESIAN_POINT('Ctrl Pts',(-26.4960084184231,22.2430930869391,-65.3557834784944));
#10909=CARTESIAN_POINT('Ctrl Pts',(-26.4884945158184,22.226232094565,-65.3546455282839));
#10910=CARTESIAN_POINT('Ctrl Pts',(-26.4829802192011,22.214062284201,-65.353819279461));
#10911=CARTESIAN_POINT('Ctrl Pts',(-26.4027771521693,22.0399459596659,-65.3419264287031));
#10912=CARTESIAN_POINT('Ctrl Pts',(-26.3148609170175,21.8844663146546,-65.3303891464609));
#10913=CARTESIAN_POINT('Ctrl Pts',(-26.0378542119916,21.4774298548182,-65.2976085076084));
#10914=CARTESIAN_POINT('Ctrl Pts',(-25.8241605116071,21.2450201493666,-65.2757082140626));
#10915=CARTESIAN_POINT('Ctrl Pts',(-25.5676911866201,21.0370236232647,-65.2548115534631));
#10916=CARTESIAN_POINT('Ctrl Pts',(-25.5550738725924,21.026947221276,-65.253795875369));
#10917=CARTESIAN_POINT('Ctrl Pts',(-25.5395659747303,21.0147521051388,-65.2525630765468));
#10918=CARTESIAN_POINT('Ctrl Pts',(-25.5367471952011,21.0125430645028,-65.2523396209909));
#10919=CARTESIAN_POINT('Ctrl Pts',(-25.5320933607234,21.0089084206918,-65.2519717278193));
#10920=CARTESIAN_POINT('Ctrl Pts',(-25.5302604459347,21.0074801034676,-65.251827096672));
#10921=CARTESIAN_POINT('Ctrl Pts',(-25.5269521579819,21.004907832985,-65.2515665249041));
#10922=CARTESIAN_POINT('Ctrl Pts',(-25.5254773392298,21.0037631821056,-65.2514505342646));
#10923=CARTESIAN_POINT('Ctrl Pts',(-25.5223030463105,21.001303935389,-65.2512012523059));
#10924=CARTESIAN_POINT('Ctrl Pts',(-25.5206032566311,20.9999897609958,-65.2510679913537));
#10925=CARTESIAN_POINT('Ctrl Pts',(-25.5159425222562,20.9963938047554,-65.2507032117953));
#10926=CARTESIAN_POINT('Ctrl Pts',(-25.5129789079462,20.9941154640748,-65.2504719388862));
#10927=CARTESIAN_POINT('Ctrl Pts',(-25.4975408665927,20.9822898246688,-65.2492706816478));
#10928=CARTESIAN_POINT('Ctrl Pts',(-25.4850004400856,20.9728284535584,-65.2483067167228));
#10929=CARTESIAN_POINT('Ctrl Pts',(-25.3610303505454,20.8807114473335,-65.2388874391317));
#10930=CARTESIAN_POINT('Ctrl Pts',(-25.2444269185878,20.8052298981961,-65.2308942656801));
#10931=CARTESIAN_POINT('Ctrl Pts',(-24.8223759056835,20.5691952039373,-65.2035513064225));
#10932=CARTESIAN_POINT('Ctrl Pts',(-24.4964249388996,20.4502922040981,-65.1848663588641));
#10933=CARTESIAN_POINT('Ctrl Pts',(-24.1374760858233,20.3813859882865,-65.1627668381719));
#10934=CARTESIAN_POINT('Ctrl Pts',(-24.1170957673541,20.3776770184089,-65.161508237918));
#10935=CARTESIAN_POINT('Ctrl Pts',(-24.0904797131951,20.373097868301,-65.1598591047469));
#10936=CARTESIAN_POINT('Ctrl Pts',(-24.0842748779539,20.3720490618765,-65.1594742684868));
#10937=CARTESIAN_POINT('Ctrl Pts',(-24.0747229152818,20.3704632508328,-65.1588812328935));
#10938=CARTESIAN_POINT('Ctrl Pts',(-24.071377921615,20.369913338812,-65.1586734444511));
#10939=CARTESIAN_POINT('Ctrl Pts',(-24.064798858475,20.3688424086849,-65.1582645318546));
#10940=CARTESIAN_POINT('Ctrl Pts',(-24.0615648493096,20.3683210417163,-65.1580634190625));
#10941=CARTESIAN_POINT('Ctrl Pts',(-24.0546797221818,20.3672218317804,-65.1576350238742));
#10942=CARTESIAN_POINT('Ctrl Pts',(-24.0510283958283,20.3666453384586,-65.157407698852));
#10943=CARTESIAN_POINT('Ctrl Pts',(-24.0406154254572,20.3650196335093,-65.1567590079164));
#10944=CARTESIAN_POINT('Ctrl Pts',(-24.0338514512466,20.3639856773472,-65.1563371580788));
#10945=CARTESIAN_POINT('Ctrl Pts',(-24.0188104367931,20.3617354718901,-65.1553980095788));
#10946=CARTESIAN_POINT('Ctrl Pts',(-24.0105318716633,20.3605298982718,-65.1548803746077));
#10947=CARTESIAN_POINT('Ctrl Pts',(-23.8049418323461,20.3314076938647,-65.1420069706271));
#10948=CARTESIAN_POINT('Ctrl Pts',(-23.6055067651159,20.3218242900325,-65.1290556153913));
#10949=CARTESIAN_POINT('Ctrl Pts',(-23.1116825070307,20.3438742037201,-65.0959819656097));
#10950=CARTESIAN_POINT('Ctrl Pts',(-22.8200766453763,20.39746684796,-65.0754908449453));
#10951=CARTESIAN_POINT('Ctrl Pts',(-22.5250321516334,20.494882873062,-65.0558376635838));
#10952=CARTESIAN_POINT('Ctrl Pts',(-22.5102644817434,20.4998778894677,-65.0548573490044));
#10953=CARTESIAN_POINT('Ctrl Pts',(-22.4921922814233,20.5061371313517,-65.0536623249617));
#10954=CARTESIAN_POINT('Ctrl Pts',(-22.4888531623401,20.50729978102,-65.0534417213696));
#10955=CARTESIAN_POINT('Ctrl Pts',(-22.4833361055669,20.5092309539891,-65.0530775608557));
#10956=CARTESIAN_POINT('Ctrl Pts',(-22.4811570803788,20.5099963233369,-65.0529338170877));
#10957=CARTESIAN_POINT('Ctrl Pts',(-22.4773949769507,20.5113222840426,-65.0526857926726));
#10958=CARTESIAN_POINT('Ctrl Pts',(-22.4758115169745,20.5118817694605,-65.05258144593));
#10959=CARTESIAN_POINT('Ctrl Pts',(-22.4722549455138,20.5131415442243,-65.0523471793031));
#10960=CARTESIAN_POINT('Ctrl Pts',(-22.4702820821845,20.5138425175052,-65.0522173011713));
#10961=CARTESIAN_POINT('Ctrl Pts',(-22.4650203324588,20.5157178339126,-65.0518710960493));
#10962=CARTESIAN_POINT('Ctrl Pts',(-22.4617326576667,20.5168956053798,-65.0516549743802));
#10963=CARTESIAN_POINT('Ctrl Pts',(-22.4463414882515,20.5224375586926,-65.0506440963381));
#10964=CARTESIAN_POINT('Ctrl Pts',(-22.4342620622151,20.5268689325222,-65.0498533118508));
#10965=CARTESIAN_POINT('Ctrl Pts',(-22.1461507940612,20.6345254099814,-65.0310464958532));
#10966=CARTESIAN_POINT('Ctrl Pts',(-21.8854918079104,20.775075804062,-65.0151415840458));
#10967=CARTESIAN_POINT('Ctrl Pts',(-21.4842623796865,21.0685740144185,-64.987165346172));
#10968=CARTESIAN_POINT('Ctrl Pts',(-21.3326171932744,21.203101399134,-64.9755360819718));
#10969=CARTESIAN_POINT('Ctrl Pts',(-21.1859237217119,21.3602232742047,-64.962474847009));
#10970=CARTESIAN_POINT('Ctrl Pts',(-21.1773113889522,21.3695578725966,-64.96170080284));
#10971=CARTESIAN_POINT('Ctrl Pts',(-21.1656315793049,21.3823683185759,-64.9606410422588));
#10972=CARTESIAN_POINT('Ctrl Pts',(-21.162516011038,21.3858003248711,-64.9603573686448));
#10973=CARTESIAN_POINT('Ctrl Pts',(-21.157229568178,21.3916489989557,-64.9598743521947));
#10974=CARTESIAN_POINT('Ctrl Pts',(-21.1550549168633,21.3940622568669,-64.9596751692562));
#10975=CARTESIAN_POINT('Ctrl Pts',(-21.150678575865,21.3989335682461,-64.959273340364));
#10976=CARTESIAN_POINT('Ctrl Pts',(-21.1484770059282,21.4013917228725,-64.9590706897684));
#10977=CARTESIAN_POINT('Ctrl Pts',(-21.1434794160074,21.4069890378138,-64.9586095157574));
#10978=CARTESIAN_POINT('Ctrl Pts',(-21.1406857592119,21.4101302914296,-64.958350893556));
#10979=CARTESIAN_POINT('Ctrl Pts',(-21.1348577956934,21.4167092682944,-64.9578096365377));
#10980=CARTESIAN_POINT('Ctrl Pts',(-21.1318246655402,21.4201480170378,-64.957526953227));
#10981=CARTESIAN_POINT('Ctrl Pts',(-21.1238931695244,21.4291789651012,-64.9567851428361));
#10982=CARTESIAN_POINT('Ctrl Pts',(-21.1190068176912,21.4347816370838,-64.9563255159311));
#10983=CARTESIAN_POINT('Ctrl Pts',(-21.104556311858,21.4514667265362,-64.9549584088274));
#10984=CARTESIAN_POINT('Ctrl Pts',(-21.0950483326351,21.4625973434099,-64.9540486105264));
#10985=CARTESIAN_POINT('Ctrl Pts',(-20.9928681589549,21.5838791806839,-64.9441581113895));
#10986=CARTESIAN_POINT('Ctrl Pts',(-20.9076128407668,21.7000406025292,-64.9348768766767));
#10987=CARTESIAN_POINT('Ctrl Pts',(-20.6865613096335,22.0478192387665,-64.9076259889112));
#10988=CARTESIAN_POINT('Ctrl Pts',(-20.5715335169468,22.2911860129293,-64.8890965198917));
#10989=CARTESIAN_POINT('Ctrl Pts',(-20.4842355155918,22.5573772704944,-64.8706368809147));
#10990=CARTESIAN_POINT('Ctrl Pts',(-20.4805589068136,22.568803254552,-64.869848058172));
#10991=CARTESIAN_POINT('Ctrl Pts',(-20.4718861830261,22.596281458557,-64.8679599148547));
#10992=CARTESIAN_POINT('Ctrl Pts',(-20.4669516178185,22.6123529205461,-64.8668628251323));
#10993=CARTESIAN_POINT('Ctrl Pts',(-20.4468774448962,22.6796038641365,-64.8623042449955));
#10994=CARTESIAN_POINT('Ctrl Pts',(-20.4328835542232,22.7311203531664,-64.8588896541004));
#10995=CARTESIAN_POINT('Ctrl Pts',(-20.4188205057784,22.7884891902786,-64.8551900844616));
#10996=CARTESIAN_POINT('Ctrl Pts',(-20.417480783404,22.7940177166079,-64.8548346145241));
#10997=CARTESIAN_POINT('Ctrl Pts',(-20.4156129516195,22.801815697793,-64.8543347328912));
#10998=CARTESIAN_POINT('Ctrl Pts',(-20.41507266458,22.8040821810121,-64.8541896217017));
#10999=CARTESIAN_POINT('Ctrl Pts',(-20.4141327293404,22.8080442170253,-64.8539362689303));
#11000=CARTESIAN_POINT('Ctrl Pts',(-20.4137319980008,22.8097395076144,-64.853827964419));
#11001=CARTESIAN_POINT('Ctrl Pts',(-20.4128911562052,22.8133096094255,-64.8536001004833));
#11002=CARTESIAN_POINT('Ctrl Pts',(-20.4124513515922,22.8151844904408,-64.8534805592613));
#11003=CARTESIAN_POINT('Ctrl Pts',(-20.4113946973694,22.8197072216796,-64.8531924898637));
#11004=CARTESIAN_POINT('Ctrl Pts',(-20.4107795155661,22.8223554680786,-64.853024058738));
#11005=CARTESIAN_POINT('Ctrl Pts',(-20.4086634809459,22.831517200304,-64.8524422019772));
#11006=CARTESIAN_POINT('Ctrl Pts',(-20.4071795281557,22.8380346319696,-64.8520297484857));
#11007=CARTESIAN_POINT('Ctrl Pts',(-20.397336533033,22.8818944054731,-64.8492636541942));
#11008=CARTESIAN_POINT('Ctrl Pts',(-20.3896224462525,22.9193803930908,-64.8469460734877));
#11009=CARTESIAN_POINT('Ctrl Pts',(-20.3668264358056,23.0410991670066,-64.8395447335085));
#11010=CARTESIAN_POINT('Ctrl Pts',(-20.3544297506129,23.1258023622658,-64.8345846477775));
#11011=CARTESIAN_POINT('Ctrl Pts',(-20.3069259080677,23.5744334521769,-64.8088491730745));
#11012=CARTESIAN_POINT('Ctrl Pts',(-20.3305580267071,23.9418344115491,-64.7892652971447));
#11013=CARTESIAN_POINT('Ctrl Pts',(-20.417050699122,24.304718952733,-64.7667666458128));
#11014=CARTESIAN_POINT('Ctrl Pts',(-20.4188069406612,24.3119754557785,-64.7663155791612));
#11015=CARTESIAN_POINT('Ctrl Pts',(-20.4251254987021,24.3376915201718,-64.7647128541929));
#11016=CARTESIAN_POINT('Ctrl Pts',(-20.4298258887457,24.3561164623674,-64.7635568390067));
#11017=CARTESIAN_POINT('Ctrl Pts',(-20.4362449131748,24.3803797054856,-64.7620239857019));
#11018=CARTESIAN_POINT('Ctrl Pts',(-20.4378174912044,24.3862565333552,-64.7616518931398));
#11019=CARTESIAN_POINT('Ctrl Pts',(-20.4402812148434,24.3953603225264,-64.7610742032586));
#11020=CARTESIAN_POINT('Ctrl Pts',(-20.4411607701951,24.3985904291168,-64.7608689831508));
#11021=CARTESIAN_POINT('Ctrl Pts',(-20.4429254534457,24.4050315002317,-64.7604592566783));
#11022=CARTESIAN_POINT('Ctrl Pts',(-20.4438105294087,24.4082424748608,-64.7602547522192));
#11023=CARTESIAN_POINT('Ctrl Pts',(-20.4457753252544,24.4153276802746,-64.7598029476627));
#11024=CARTESIAN_POINT('Ctrl Pts',(-20.4468573216618,24.4192012690255,-64.7595555736223));
#11025=CARTESIAN_POINT('Ctrl Pts',(-20.4499917991371,24.4303422890537,-64.7588430304223));
#11026=CARTESIAN_POINT('Ctrl Pts',(-20.4520625668063,24.4376045085088,-64.7583772650268));
#11027=CARTESIAN_POINT('Ctrl Pts',(-20.4567799190851,24.4539305242151,-64.7573272388287));
#11028=CARTESIAN_POINT('Ctrl Pts',(-20.4594408427573,24.4629900731631,-64.7567425116486));
#11029=CARTESIAN_POINT('Ctrl Pts',(-20.4679297547791,24.4914291314351,-64.7549004533933));
#11030=CARTESIAN_POINT('Ctrl Pts',(-20.4739004014279,24.5107652247049,-64.7536384597835));
#11031=CARTESIAN_POINT('Ctrl Pts',(-20.4971994900216,24.5837735138577,-64.7488365415595));
#11032=CARTESIAN_POINT('Ctrl Pts',(-20.5157528873839,24.6370412701138,-64.7452567628918));
#11033=CARTESIAN_POINT('Ctrl Pts',(-20.5925692038498,24.8402525517416,-64.7312979845225));
#11034=CARTESIAN_POINT('Ctrl Pts',(-20.6606224119458,24.9862249375739,-64.7206110241176));
#11035=CARTESIAN_POINT('Ctrl Pts',(-20.8640342690094,25.3489780177236,-64.6925706915598));
#11036=CARTESIAN_POINT('Ctrl Pts',(-21.0147722782517,25.5558800523545,-64.6750341957923));
#11037=CARTESIAN_POINT('Ctrl Pts',(-21.1906876975557,25.7453796934671,-64.6586885307075));
#11038=CARTESIAN_POINT('Ctrl Pts',(-21.1930387648057,25.7479041693053,-64.6584707341213));
#11039=CARTESIAN_POINT('Ctrl Pts',(-21.2036191260345,25.7592283980989,-64.6574935744861));
#11040=CARTESIAN_POINT('Ctrl Pts',(-21.2118938171755,25.7679858907968,-64.6567374252627));
#11041=CARTESIAN_POINT('Ctrl Pts',(-21.222679295567,25.7792731888629,-64.6557624772415));
#11042=CARTESIAN_POINT('Ctrl Pts',(-21.2251452963097,25.7818453717697,-64.6555402782733));
#11043=CARTESIAN_POINT('Ctrl Pts',(-21.2289320158149,25.7857820508649,-64.6552001761265));
#11044=CARTESIAN_POINT('Ctrl Pts',(-21.2302496727268,25.7871494678431,-64.6550820349613));
#11045=CARTESIAN_POINT('Ctrl Pts',(-21.2328507938901,25.7898440472917,-64.6548492207611));
#11046=CARTESIAN_POINT('Ctrl Pts',(-21.2341341832591,25.7911712645339,-64.6547345434827));
#11047=CARTESIAN_POINT('Ctrl Pts',(-21.2369959845428,25.7941257118783,-64.6544792560685));
#11048=CARTESIAN_POINT('Ctrl Pts',(-21.2385749694671,25.7957523758403,-64.6543386921994));
#11049=CARTESIAN_POINT('Ctrl Pts',(-21.2431414655628,25.800446840543,-64.6539330063323));
#11050=CARTESIAN_POINT('Ctrl Pts',(-21.2461333910172,25.8035103698279,-64.6536682302395));
#11051=CARTESIAN_POINT('Ctrl Pts',(-21.2663911048564,25.8241703592835,-64.651882324415));
#11052=CARTESIAN_POINT('Ctrl Pts',(-21.283852813003,25.8415747935159,-64.6503763881162));
#11053=CARTESIAN_POINT('Ctrl Pts',(-21.3384865036833,25.8947935886847,-64.6457603629969));
#11054=CARTESIAN_POINT('Ctrl Pts',(-21.3763220456454,25.9299181847254,-64.642697665052));
#11055=CARTESIAN_POINT('Ctrl Pts',(-21.5397509046883,26.074484470923,-64.6299394068529));
#11056=CARTESIAN_POINT('Ctrl Pts',(-21.6728939802513,26.1750187877095,-64.6206709613844));
#11057=CARTESIAN_POINT('Ctrl Pts',(-21.8981479585447,26.3191572699258,-64.6057278828375));
#11058=CARTESIAN_POINT('Ctrl Pts',(-21.9855177837693,26.3694475531502,-64.6000934786598));
#11059=CARTESIAN_POINT('Ctrl Pts',(-22.0750364910777,26.4155370194908,-64.5943742034087));
#11060=CARTESIAN_POINT('Origin',(-23.5502525316942,23.5502525316942,-77.3107734492734));
#11061=CARTESIAN_POINT('',(-22.0750360104957,26.415536772059,-63.0988976931332));
#11062=CARTESIAN_POINT('',(-22.0750360636209,26.415536799411,-63.3454515897691));
#11063=CARTESIAN_POINT('',(-22.0750360153461,26.4155367745563,-77.3107734492734));
#11064=CARTESIAN_POINT('',(-26.7730015586105,23.5477481335051,-63.9376071674064));
#11065=CARTESIAN_POINT('Ctrl Pts',(-22.0750360104957,26.415536772059,-63.0988976931332));
#11066=CARTESIAN_POINT('Ctrl Pts',(-22.0301551534622,26.3924294723194,-63.1018341048178));
#11067=CARTESIAN_POINT('Ctrl Pts',(-21.9858167660497,26.3682674425502,-63.1047303870157));
#11068=CARTESIAN_POINT('Ctrl Pts',(-21.645912760162,26.1725397346903,-63.1270342225087));
#11069=CARTESIAN_POINT('Ctrl Pts',(-21.3787938250415,25.9560113334665,-63.1454359720157));
#11070=CARTESIAN_POINT('Ctrl Pts',(-21.1475892577515,25.6981231034343,-63.166177027197));
#11071=CARTESIAN_POINT('Ctrl Pts',(-21.1445202841832,25.6946851265449,-63.1664532973355));
#11072=CARTESIAN_POINT('Ctrl Pts',(-21.1388395952117,25.6882938678697,-63.1669664628214));
#11073=CARTESIAN_POINT('Ctrl Pts',(-21.1362259013136,25.6853423501882,-63.1672032778995));
#11074=CARTESIAN_POINT('Ctrl Pts',(-21.120110041865,25.6670760700166,-63.1686678573895));
#11075=CARTESIAN_POINT('Ctrl Pts',(-21.1067484835751,25.6516383484345,-63.1699012468026));
#11076=CARTESIAN_POINT('Ctrl Pts',(-21.0844261845881,25.6253467582129,-63.1719950409862));
#11077=CARTESIAN_POINT('Ctrl Pts',(-21.0753881122835,25.6145591268285,-63.1728522528438));
#11078=CARTESIAN_POINT('Ctrl Pts',(-21.0629948840193,25.5995684835867,-63.1740409946307));
#11079=CARTESIAN_POINT('Ctrl Pts',(-21.0595790639225,25.5954156432777,-63.1743700526592));
#11080=CARTESIAN_POINT('Ctrl Pts',(-21.0541428008188,25.5887725971272,-63.1748960246155));
#11081=CARTESIAN_POINT('Ctrl Pts',(-21.0521156432332,25.5862878781786,-63.175092666101));
#11082=CARTESIAN_POINT('Ctrl Pts',(-21.0481707408952,25.5814377884834,-63.1754763317806));
#11083=CARTESIAN_POINT('Ctrl Pts',(-21.0462526327908,25.5790727162945,-63.1756633410165));
#11084=CARTESIAN_POINT('Ctrl Pts',(-21.0417132680198,25.5734593297433,-63.1761070124693));
#11085=CARTESIAN_POINT('Ctrl Pts',(-21.0390949693512,25.5702086405962,-63.1763637934765));
#11086=CARTESIAN_POINT('Ctrl Pts',(-21.0313260701538,25.5605248905896,-63.1771283089979));
#11087=CARTESIAN_POINT('Ctrl Pts',(-21.0261938506064,25.5540771866951,-63.1776367804371));
#11088=CARTESIAN_POINT('Ctrl Pts',(-21.0145642430654,25.5393511246037,-63.1787968466262));
#11089=CARTESIAN_POINT('Ctrl Pts',(-21.0080825853661,25.5310605156137,-63.1794490631095));
#11090=CARTESIAN_POINT('Ctrl Pts',(-20.9512170781906,25.4575856937487,-63.1852217288918));
#11091=CARTESIAN_POINT('Ctrl Pts',(-20.9033134590413,25.3905287658824,-63.1904391755171));
#11092=CARTESIAN_POINT('Ctrl Pts',(-20.794074657468,25.224510763073,-63.2032510446905));
#11093=CARTESIAN_POINT('Ctrl Pts',(-20.7354321874675,25.1239230542687,-63.2109310196733));
#11094=CARTESIAN_POINT('Ctrl Pts',(-20.5498436287947,24.7618843991332,-63.2381773223736));
#11095=CARTESIAN_POINT('Ctrl Pts',(-20.4528852974654,24.486645597089,-63.2583274810434));
#11096=CARTESIAN_POINT('Ctrl Pts',(-20.3908918254272,24.1865012295665,-63.2777193655171));
#11097=CARTESIAN_POINT('Ctrl Pts',(-20.3877784341178,24.170841030711,-63.2787235959971));
#11098=CARTESIAN_POINT('Ctrl Pts',(-20.384112053227,24.1516548537664,-63.2799441681011));
#11099=CARTESIAN_POINT('Ctrl Pts',(-20.3834484390684,24.1481506180055,-63.2801667002449));
#11100=CARTESIAN_POINT('Ctrl Pts',(-20.3823629216087,24.1423659995565,-63.2805333808749));
#11101=CARTESIAN_POINT('Ctrl Pts',(-20.3819376625254,24.1400862628306,-63.280677720726));
#11102=CARTESIAN_POINT('Ctrl Pts',(-20.3811745796632,24.1359708770974,-63.2809379738082));
#11103=CARTESIAN_POINT('Ctrl Pts',(-20.3808358906848,24.1341353983216,-63.2810539365173));
#11104=CARTESIAN_POINT('Ctrl Pts',(-20.3801101745535,24.130183241356,-63.2813033879504));
#11105=CARTESIAN_POINT('Ctrl Pts',(-20.3797236737425,24.1280664753704,-63.2814368458983));
#11106=CARTESIAN_POINT('Ctrl Pts',(-20.3786688956442,24.122256802769,-63.2818027332029));
#11107=CARTESIAN_POINT('Ctrl Pts',(-20.3780049457602,24.1185630986069,-63.2820349143377));
#11108=CARTESIAN_POINT('Ctrl Pts',(-20.3745618554222,24.0992143644919,-63.2832488612489));
#11109=CARTESIAN_POINT('Ctrl Pts',(-20.3718920807936,24.0835397281584,-63.2842244548524));
#11110=CARTESIAN_POINT('Ctrl Pts',(-20.3400262407354,23.8877053765299,-63.2963227657731));
#11111=CARTESIAN_POINT('Ctrl Pts',(-20.3260649266678,23.7053714613306,-63.306642365193));
#11112=CARTESIAN_POINT('Ctrl Pts',(-20.3296240298868,23.2873739331184,-63.330059540505));
#11113=CARTESIAN_POINT('Ctrl Pts',(-20.3574216320898,23.0528845765,-63.34306672695));
#11114=CARTESIAN_POINT('Ctrl Pts',(-20.4131995793952,22.8119040354237,-63.3575855399289));
#11115=CARTESIAN_POINT('Ctrl Pts',(-20.4159527103446,22.8003029652243,-63.3582871898052));
#11116=CARTESIAN_POINT('Ctrl Pts',(-20.4349444715038,22.7222075832218,-63.3630294085441));
#11117=CARTESIAN_POINT('Ctrl Pts',(-20.4532325950998,22.6562339640932,-63.3671286051469));
#11118=CARTESIAN_POINT('Ctrl Pts',(-20.4764095696033,22.5819056447239,-63.3718709218751));
#11119=CARTESIAN_POINT('Ctrl Pts',(-20.4792523221489,22.5729276322311,-63.3724458130778));
#11120=CARTESIAN_POINT('Ctrl Pts',(-20.4834732769373,22.5597972295947,-63.3732896793406));
#11121=CARTESIAN_POINT('Ctrl Pts',(-20.4848206672027,22.5556349234018,-63.3735576380188));
#11122=CARTESIAN_POINT('Ctrl Pts',(-20.4872253688208,22.5482577135852,-63.374033376593));
#11123=CARTESIAN_POINT('Ctrl Pts',(-20.4882792786965,22.5450417011689,-63.3742410438714));
#11124=CARTESIAN_POINT('Ctrl Pts',(-20.490318407154,22.5388522509025,-63.374641245611));
#11125=CARTESIAN_POINT('Ctrl Pts',(-20.4913028993855,22.5358785762917,-63.3748337558462));
#11126=CARTESIAN_POINT('Ctrl Pts',(-20.4939334536495,22.5279716002884,-63.3753462704954));
#11127=CARTESIAN_POINT('Ctrl Pts',(-20.4955871195197,22.523040855021,-63.375666526439));
#11128=CARTESIAN_POINT('Ctrl Pts',(-20.5017791887359,22.5047251071461,-63.3768586006951));
#11129=CARTESIAN_POINT('Ctrl Pts',(-20.5063936410173,22.4913661536413,-63.3777329386884));
#11130=CARTESIAN_POINT('Ctrl Pts',(-20.5179214612466,22.4586909222095,-63.3798836805679));
#11131=CARTESIAN_POINT('Ctrl Pts',(-20.5249316231792,22.4394096817924,-63.381163285861));
#11132=CARTESIAN_POINT('Ctrl Pts',(-20.5522694506815,22.3663964155993,-63.3860494806778));
#11133=CARTESIAN_POINT('Ctrl Pts',(-20.5738474612456,22.3131470245561,-63.3896974630876));
#11134=CARTESIAN_POINT('Ctrl Pts',(-20.6641086150541,22.106456293385,-63.4041984933293));
#11135=CARTESIAN_POINT('Ctrl Pts',(-20.7433222049716,21.9579261622564,-63.415390190971));
#11136=CARTESIAN_POINT('Ctrl Pts',(-20.9666127783519,21.6081132263309,-63.4434029360249));
#11137=CARTESIAN_POINT('Ctrl Pts',(-21.1229747383331,21.4159041668097,-63.460341833443));
#11138=CARTESIAN_POINT('Ctrl Pts',(-21.3100590745428,21.2333887920073,-63.4768563215546));
#11139=CARTESIAN_POINT('Ctrl Pts',(-21.3204186712893,21.2234166356407,-63.4777599426763));
#11140=CARTESIAN_POINT('Ctrl Pts',(-21.333575863148,21.2109200850646,-63.4788935715632));
#11141=CARTESIAN_POINT('Ctrl Pts',(-21.3363113955375,21.2083310140703,-63.4791285090593));
#11142=CARTESIAN_POINT('Ctrl Pts',(-21.3406354177513,21.2042528486557,-63.4794986698731));
#11143=CARTESIAN_POINT('Ctrl Pts',(-21.3422208774871,21.2027605685273,-63.4796341401154));
#11144=CARTESIAN_POINT('Ctrl Pts',(-21.3451668380155,21.1999933710111,-63.4798853855385));
#11145=CARTESIAN_POINT('Ctrl Pts',(-21.3465269245834,21.1987180353626,-63.4800011931034));
#11146=CARTESIAN_POINT('Ctrl Pts',(-21.3495572592048,21.1958814676431,-63.4802588021786));
#11147=CARTESIAN_POINT('Ctrl Pts',(-21.3512280582278,21.1943208360009,-63.4804005568849));
#11148=CARTESIAN_POINT('Ctrl Pts',(-21.356099897741,21.189779928584,-63.4808130856425));
#11149=CARTESIAN_POINT('Ctrl Pts',(-21.3593053622352,21.1868043743838,-63.4810834954298));
#11150=CARTESIAN_POINT('Ctrl Pts',(-21.3821099214642,21.1657217238201,-63.4830001448988));
#11151=CARTESIAN_POINT('Ctrl Pts',(-21.4019279220865,21.1478514337128,-63.4846285318492));
#11152=CARTESIAN_POINT('Ctrl Pts',(-21.4293547842209,21.1237309231788,-63.4868354429079));
#11153=CARTESIAN_POINT('Ctrl Pts',(-21.4367730196159,21.1172669729836,-63.4874277685858));
#11154=CARTESIAN_POINT('Ctrl Pts',(-21.518271278153,21.0469067107706,-63.4938867041588));
#11155=CARTESIAN_POINT('Ctrl Pts',(-21.5952013215871,20.9863753187256,-63.4995480745962));
#11156=CARTESIAN_POINT('Ctrl Pts',(-21.8691045028307,20.7903679702629,-63.5187110824417));
#11157=CARTESIAN_POINT('Ctrl Pts',(-22.0782987305988,20.6733480545255,-63.5317373458434));
#11158=CARTESIAN_POINT('Ctrl Pts',(-22.3508088361478,20.5584849682122,-63.5486955513083));
#11159=CARTESIAN_POINT('Ctrl Pts',(-22.4036759750995,20.5378282490587,-63.551981546353));
#11160=CARTESIAN_POINT('Ctrl Pts',(-22.4743062501571,20.5123596262334,-63.5563836432989));
#11161=CARTESIAN_POINT('Ctrl Pts',(-22.4916059411943,20.5062878335387,-63.5574627779333));
#11162=CARTESIAN_POINT('Ctrl Pts',(-22.51313020436,20.4989389959765,-63.5588070250674));
#11163=CARTESIAN_POINT('Ctrl Pts',(-22.5173070516366,20.4975224994001,-63.5590679539582));
#11164=CARTESIAN_POINT('Ctrl Pts',(-22.525281552246,20.494836342695,-63.5595662731713));
#11165=CARTESIAN_POINT('Ctrl Pts',(-22.5290786922107,20.4935651767198,-63.559803617626));
#11166=CARTESIAN_POINT('Ctrl Pts',(-22.537986211887,20.4906016626653,-63.5603605518315));
#11167=CARTESIAN_POINT('Ctrl Pts',(-22.543098472267,20.4889150392498,-63.560680314175));
#11168=CARTESIAN_POINT('Ctrl Pts',(-22.5547584423909,20.4851005809968,-63.5614099229132));
#11169=CARTESIAN_POINT('Ctrl Pts',(-22.5613087780052,20.4829809079735,-63.5618200170746));
#11170=CARTESIAN_POINT('Ctrl Pts',(-22.5709033461129,20.4799100578105,-63.5624210387485));
#11171=CARTESIAN_POINT('Ctrl Pts',(-22.5739423065505,20.4789423750337,-63.5626114544927));
#11172=CARTESIAN_POINT('Ctrl Pts',(-22.5781209528972,20.4776186157072,-63.5628733512343));
#11173=CARTESIAN_POINT('Ctrl Pts',(-22.5792594144885,20.4772586569035,-63.5629447115072));
#11174=CARTESIAN_POINT('Ctrl Pts',(-22.5869333763851,20.474836993768,-63.5634257744358));
#11175=CARTESIAN_POINT('Ctrl Pts',(-22.5934752019205,20.4727955188241,-63.5638361053001));
#11176=CARTESIAN_POINT('Ctrl Pts',(-22.6058354316685,20.4689815440914,-63.5646118708173));
#11177=CARTESIAN_POINT('Ctrl Pts',(-22.6116524466462,20.4672046181105,-63.5649771643711));
#11178=CARTESIAN_POINT('Ctrl Pts',(-22.6422131915426,20.4579637219404,-63.5668974040785));
#11179=CARTESIAN_POINT('Ctrl Pts',(-22.6670404706536,20.4507812990952,-63.5684611938968));
#11180=CARTESIAN_POINT('Ctrl Pts',(-22.7005903620495,20.4415112914972,-63.570580454431));
#11181=CARTESIAN_POINT('Ctrl Pts',(-22.7092396672428,20.4391602379326,-63.5711273471674));
#11182=CARTESIAN_POINT('Ctrl Pts',(-22.7221781777228,20.4357011915164,-63.5719462868049));
#11183=CARTESIAN_POINT('Ctrl Pts',(-22.7264600932906,20.4345658971915,-63.5722174469699));
#11184=CARTESIAN_POINT('Ctrl Pts',(-22.7338322466006,20.4326275261675,-63.5726845435035));
#11185=CARTESIAN_POINT('Ctrl Pts',(-22.7369213705381,20.4318202045176,-63.5728803419315));
#11186=CARTESIAN_POINT('Ctrl Pts',(-22.7432931448948,20.4301650962022,-63.5732843573954));
#11187=CARTESIAN_POINT('Ctrl Pts',(-22.7465759419849,20.4293178966731,-63.5734925931475));
#11188=CARTESIAN_POINT('Ctrl Pts',(-22.7530747789813,20.4276516595302,-63.5739049971667));
#11189=CARTESIAN_POINT('Ctrl Pts',(-22.7562907594769,20.4268324061931,-63.5741091581341));
#11190=CARTESIAN_POINT('Ctrl Pts',(-22.7668823262403,20.4241516778889,-63.5747818152304));
#11191=CARTESIAN_POINT('Ctrl Pts',(-22.7742631962656,20.4223113595066,-63.5752509954441));
#11192=CARTESIAN_POINT('Ctrl Pts',(-22.82362788675,20.4101884299898,-63.5783919213651));
#11193=CARTESIAN_POINT('Ctrl Pts',(-22.8658067062213,20.4007256535867,-63.5810900011819));
#11194=CARTESIAN_POINT('Ctrl Pts',(-22.9873382356944,20.3760166943649,-63.588909847546));
#11195=CARTESIAN_POINT('Ctrl Pts',(-23.0670861971151,20.3629034583346,-63.5940974776461));
#11196=CARTESIAN_POINT('Ctrl Pts',(-23.2491804851409,20.339951813884,-63.606070421336));
#11197=CARTESIAN_POINT('Ctrl Pts',(-23.3516723458384,20.3319862064312,-63.6129009116404));
#11198=CARTESIAN_POINT('Ctrl Pts',(-23.7098477013597,20.3213243303132,-63.6369805722327));
#11199=CARTESIAN_POINT('Ctrl Pts',(-23.9653350569952,20.3441388637953,-63.6546005567174));
#11200=CARTESIAN_POINT('Ctrl Pts',(-24.2235464293843,20.3986082982474,-63.6715136187067));
#11201=CARTESIAN_POINT('Ctrl Pts',(-24.2316372395491,20.4003476236201,-63.6720425604478));
#11202=CARTESIAN_POINT('Ctrl Pts',(-24.2640491440968,20.4074461126367,-63.6741572025787));
#11203=CARTESIAN_POINT('Ctrl Pts',(-24.2883152796707,20.4130561297622,-63.6757306606294));
#11204=CARTESIAN_POINT('Ctrl Pts',(-24.3165523130673,20.4199299485038,-63.6775482663191));
#11205=CARTESIAN_POINT('Ctrl Pts',(-24.3205879172099,20.4209206183223,-63.6778077173996));
#11206=CARTESIAN_POINT('Ctrl Pts',(-24.3270208478082,20.422512987778,-63.6782207722871));
#11207=CARTESIAN_POINT('Ctrl Pts',(-24.3294194004502,20.4231096404551,-63.6783746662615));
#11208=CARTESIAN_POINT('Ctrl Pts',(-24.3336504637385,20.4241673100229,-63.6786459290528));
#11209=CARTESIAN_POINT('Ctrl Pts',(-24.3354832568803,20.4246271796436,-63.6787633647369));
#11210=CARTESIAN_POINT('Ctrl Pts',(-24.3392954315849,20.4255872643828,-63.6790074845737));
#11211=CARTESIAN_POINT('Ctrl Pts',(-24.3412747386611,20.4260877475077,-63.6791341526239));
#11212=CARTESIAN_POINT('Ctrl Pts',(-24.3464133462509,20.42739228066,-63.6794627975166));
#11213=CARTESIAN_POINT('Ctrl Pts',(-24.3495719147223,20.4281992467126,-63.6796646044222));
#11214=CARTESIAN_POINT('Ctrl Pts',(-24.3630343989446,20.4316604753123,-63.6805239051905));
#11215=CARTESIAN_POINT('Ctrl Pts',(-24.373326514114,20.4343610052092,-63.6811787371725));
#11216=CARTESIAN_POINT('Ctrl Pts',(-24.5381911313162,20.478493415982,-63.6916371404394));
#11217=CARTESIAN_POINT('Ctrl Pts',(-24.6895045606705,20.5313376831255,-63.7008021472877));
#11218=CARTESIAN_POINT('Ctrl Pts',(-24.9169516437348,20.6303225793272,-63.7147716447462));
#11219=CARTESIAN_POINT('Ctrl Pts',(-24.9961494052048,20.668718212602,-63.719673817853));
#11220=CARTESIAN_POINT('Ctrl Pts',(-25.1652820033998,20.7594455967726,-63.7304045938781));
#11221=CARTESIAN_POINT('Ctrl Pts',(-25.254452193926,20.8129864247453,-63.7362342701892));
#11222=CARTESIAN_POINT('Ctrl Pts',(-25.3932382584673,20.9057322787311,-63.7457659596978));
#11223=CARTESIAN_POINT('Ctrl Pts',(-25.4445610543022,20.9422497783605,-63.7493982772262));
#11224=CARTESIAN_POINT('Ctrl Pts',(-25.5131049775109,20.9941117043254,-63.7544241880185));
#11225=CARTESIAN_POINT('Ctrl Pts',(-25.5312815800207,21.0081727676195,-63.7557743522765));
#11226=CARTESIAN_POINT('Ctrl Pts',(-25.553206854687,21.0255116982045,-63.7574251861631));
#11227=CARTESIAN_POINT('Ctrl Pts',(-25.5571006024925,21.0286056260707,-63.7577192230305));
#11228=CARTESIAN_POINT('Ctrl Pts',(-25.5640949401086,21.0341897083405,-63.758248968692));
#11229=CARTESIAN_POINT('Ctrl Pts',(-25.5671981170502,21.0366766162889,-63.7584845587877));
#11230=CARTESIAN_POINT('Ctrl Pts',(-25.5805503230972,21.047417815452,-63.7595006675458));
#11231=CARTESIAN_POINT('Ctrl Pts',(-25.5907532432506,21.0557290145861,-63.7602832805404));
#11232=CARTESIAN_POINT('Ctrl Pts',(-25.6023887222068,21.0653263118808,-63.7611830175948));
#11233=CARTESIAN_POINT('Ctrl Pts',(-25.6038714788543,21.0665515669705,-63.7612978103889));
#11234=CARTESIAN_POINT('Ctrl Pts',(-25.6099606158738,21.0715924202583,-63.761769781487));
#11235=CARTESIAN_POINT('Ctrl Pts',(-25.6145574455267,21.0754194944818,-63.7621274002556));
#11236=CARTESIAN_POINT('Ctrl Pts',(-25.6220054196052,21.081655467448,-63.76270898971));
#11237=CARTESIAN_POINT('Ctrl Pts',(-25.6248630937489,21.0840565723653,-63.7629326560072));
#11238=CARTESIAN_POINT('Ctrl Pts',(-25.6341478867354,21.0918854962583,-63.7636610643951));
#11239=CARTESIAN_POINT('Ctrl Pts',(-25.6405578880618,21.0973334855759,-63.7641665985672));
#11240=CARTESIAN_POINT('Ctrl Pts',(-25.668258817615,21.1210644969308,-63.7663629553014));
#11241=CARTESIAN_POINT('Ctrl Pts',(-25.6893312579413,21.1395996613051,-63.7680638507021));
#11242=CARTESIAN_POINT('Ctrl Pts',(-25.7148729846291,21.162664583735,-63.7701639051844));
#11243=CARTESIAN_POINT('Ctrl Pts',(-25.7195748967614,21.1669358531951,-63.7705521220615));
#11244=CARTESIAN_POINT('Ctrl Pts',(-25.7273283587484,21.1740211380327,-63.771194998021));
#11245=CARTESIAN_POINT('Ctrl Pts',(-25.7303871696702,21.17682721098,-63.7714493190161));
#11246=CARTESIAN_POINT('Ctrl Pts',(-25.7359039553514,21.1819078287484,-63.7719092775714));
#11247=CARTESIAN_POINT('Ctrl Pts',(-25.7383638261394,21.184180313715,-63.7721148269393));
#11248=CARTESIAN_POINT('Ctrl Pts',(-25.7431293325022,21.1885965849534,-63.7725139320604));
#11249=CARTESIAN_POINT('Ctrl Pts',(-25.7454353784346,21.1907399244886,-63.7727074685279));
#11250=CARTESIAN_POINT('Ctrl Pts',(-25.7504736057915,21.1954364515697,-63.7731312011814));
#11251=CARTESIAN_POINT('Ctrl Pts',(-25.7532044888232,21.1979910197642,-63.773361456652));
#11252=CARTESIAN_POINT('Ctrl Pts',(-25.7643598815582,21.2084626482572,-63.7743044054872));
#11253=CARTESIAN_POINT('Ctrl Pts',(-25.7727461268446,21.2164201836428,-63.775018845801));
#11254=CARTESIAN_POINT('Ctrl Pts',(-25.8616075729008,21.3016522877886,-63.7826491241886));
#11255=CARTESIAN_POINT('Ctrl Pts',(-25.9380520132177,21.3830022284673,-63.7897446784749));
#11256=CARTESIAN_POINT('Ctrl Pts',(-26.0539064112616,21.5198761086836,-63.8014145119917));
#11257=CARTESIAN_POINT('Ctrl Pts',(-26.0960491169722,21.57297409619,-63.8058817119423));
#11258=CARTESIAN_POINT('Ctrl Pts',(-26.324513739653,21.8802518529808,-63.8313665341198));
#11259=CARTESIAN_POINT('Ctrl Pts',(-26.4744259188162,22.1593411357999,-63.8533463801359));
#11260=CARTESIAN_POINT('Ctrl Pts',(-26.5869938083489,22.4710924935984,-63.8743247543954));
#11261=CARTESIAN_POINT('Ctrl Pts',(-26.5924205168948,22.4864866054808,-63.8753515643297));
#11262=CARTESIAN_POINT('Ctrl Pts',(-26.5988996404045,22.5053212927182,-63.876596225667));
#11263=CARTESIAN_POINT('Ctrl Pts',(-26.6000634285163,22.5087228962198,-63.8768205538468));
#11264=CARTESIAN_POINT('Ctrl Pts',(-26.6019714253797,22.5143303454824,-63.8771895842546));
#11265=CARTESIAN_POINT('Ctrl Pts',(-26.6027189362507,22.5165350504218,-63.8773344820882));
#11266=CARTESIAN_POINT('Ctrl Pts',(-26.6040616743462,22.5205094720401,-63.8775953348541));
#11267=CARTESIAN_POINT('Ctrl Pts',(-26.6046577511417,22.5222788918951,-63.8777113403204));
#11268=CARTESIAN_POINT('Ctrl Pts',(-26.6059353968032,22.5260824323006,-63.877960432883));
#11269=CARTESIAN_POINT('Ctrl Pts',(-26.6066164705472,22.5281167100166,-63.8780934900129));
#11270=CARTESIAN_POINT('Ctrl Pts',(-26.608474146703,22.5336838025361,-63.8784571670253));
#11271=CARTESIAN_POINT('Ctrl Pts',(-26.6096466630747,22.537217992887,-63.878687543676));
#11272=CARTESIAN_POINT('Ctrl Pts',(-26.6156764187877,22.5554987886701,-63.8798766420982));
#11273=CARTESIAN_POINT('Ctrl Pts',(-26.6204332807995,22.5702786506548,-63.8808294886697));
#11274=CARTESIAN_POINT('Ctrl Pts',(-26.6469165927349,22.6546498556362,-63.886223442358));
#11275=CARTESIAN_POINT('Ctrl Pts',(-26.6663853187895,22.7249339655637,-63.8905415926922));
#11276=CARTESIAN_POINT('Ctrl Pts',(-26.7427465550266,23.0420681797853,-63.9094968911549));
#11277=CARTESIAN_POINT('Ctrl Pts',(-26.772804718694,23.2944474994768,-63.9232316158934));
#11278=CARTESIAN_POINT('Ctrl Pts',(-26.7730015586105,23.5477481335051,-63.9376071674064));
#11279=CARTESIAN_POINT('Ctrl Pts',(-26.7730015615053,23.5477518614343,-63.9376073789773));
#11280=CARTESIAN_POINT('Ctrl Pts',(-26.7731347904089,23.7194511561076,-63.9473518193325));
#11281=CARTESIAN_POINT('Ctrl Pts',(-26.7595469903421,23.8908673797861,-63.9573375528294));
#11282=CARTESIAN_POINT('Ctrl Pts',(-26.7312784852756,24.0672044259549,-63.9682105578638));
#11283=CARTESIAN_POINT('Ctrl Pts',(-26.7301619710957,24.0740285662475,-63.9686322487113));
#11284=CARTESIAN_POINT('Ctrl Pts',(-26.7283045162005,24.0851564644852,-63.9693213939651));
#11285=CARTESIAN_POINT('Ctrl Pts',(-26.7275767709856,24.0894624274258,-63.9695884289721));
#11286=CARTESIAN_POINT('Ctrl Pts',(-26.7262793924432,24.097044999596,-63.9700593184265));
#11287=CARTESIAN_POINT('Ctrl Pts',(-26.72571343387,24.1003222379813,-63.9702630557172));
#11288=CARTESIAN_POINT('Ctrl Pts',(-26.7245596525089,24.1069421980216,-63.9706750396583));
#11289=CARTESIAN_POINT('Ctrl Pts',(-26.7239716201346,24.1102848784175,-63.9708832927453));
#11290=CARTESIAN_POINT('Ctrl Pts',(-26.7228213350131,24.1167636986026,-63.9712873719911));
#11291=CARTESIAN_POINT('Ctrl Pts',(-26.7222597094878,24.1198999471429,-63.9714831779299));
#11292=CARTESIAN_POINT('Ctrl Pts',(-26.720910637082,24.1273696255038,-63.9719500136222));
#11293=CARTESIAN_POINT('Ctrl Pts',(-26.7201189572045,24.1317022761708,-63.9722211782684));
#11294=CARTESIAN_POINT('Ctrl Pts',(-26.717270713963,24.1471112334778,-63.9731869478697));
#11295=CARTESIAN_POINT('Ctrl Pts',(-26.7151649750293,24.1581782652703,-63.9738831220685));
#11296=CARTESIAN_POINT('Ctrl Pts',(-26.6831920253362,24.3215473243091,-63.9841980127897));
#11297=CARTESIAN_POINT('Ctrl Pts',(-26.642424015365,24.4714843332734,-63.9941703802944));
#11298=CARTESIAN_POINT('Ctrl Pts',(-26.5844352657248,24.6366447535082,-64.0057368878791));
#11299=CARTESIAN_POINT('Ctrl Pts',(-26.5776748125846,24.6553440372302,-64.0070548570558));
#11300=CARTESIAN_POINT('Ctrl Pts',(-26.5022367382458,24.8581156530629,-64.0214362764283));
#11301=CARTESIAN_POINT('Ctrl Pts',(-26.4170379823137,25.0355977637447,-64.0348663633243));
#11302=CARTESIAN_POINT('Ctrl Pts',(-26.2463000278234,25.3211298096228,-64.0571914078849));
#11303=CARTESIAN_POINT('Ctrl Pts',(-26.1690266904687,25.4335237533714,-64.0661829110351));
#11304=CARTESIAN_POINT('Ctrl Pts',(-26.0812741598373,25.5452665118788,-64.0750823080167));
#11305=CARTESIAN_POINT('Ctrl Pts',(-26.0776763427416,25.5498225214328,-64.0754450754333));
#11306=CARTESIAN_POINT('Ctrl Pts',(-26.0724700428257,25.5563788929013,-64.0759669709197));
#11307=CARTESIAN_POINT('Ctrl Pts',(-26.0708714769055,25.5583870599916,-64.0761268033778));
#11308=CARTESIAN_POINT('Ctrl Pts',(-26.0680866670928,25.5618768583202,-64.0764045222856));
#11309=CARTESIAN_POINT('Ctrl Pts',(-26.0669015120199,25.56335935319,-64.0765224874309));
#11310=CARTESIAN_POINT('Ctrl Pts',(-26.0646046887291,25.5662272210027,-64.0767506648602));
#11311=CARTESIAN_POINT('Ctrl Pts',(-26.0634931876341,25.5676127183956,-64.0768608888079));
#11312=CARTESIAN_POINT('Ctrl Pts',(-26.0608372118056,25.5709178173695,-64.0771238033051));
#11313=CARTESIAN_POINT('Ctrl Pts',(-26.0592916773286,25.5728365716076,-64.0772764170272));
#11314=CARTESIAN_POINT('Ctrl Pts',(-26.0546126822582,25.578631846478,-64.0777373082798));
#11315=CARTESIAN_POINT('Ctrl Pts',(-26.0514724082362,25.5825028948026,-64.0780450964729));
#11316=CARTESIAN_POINT('Ctrl Pts',(-26.0193083197012,25.6219644174305,-64.0811821430463));
#11317=CARTESIAN_POINT('Ctrl Pts',(-25.9895340573297,25.6569401673688,-64.0839580083613));
#11318=CARTESIAN_POINT('Ctrl Pts',(-25.780569757103,25.8920370752181,-64.1026800415497));
#11319=CARTESIAN_POINT('Ctrl Pts',(-25.5776967119744,26.0697324670794,-64.1172252101184));
#11320=CARTESIAN_POINT('Ctrl Pts',(-25.271731464199,26.2765602915612,-64.1380555047595));
#11321=CARTESIAN_POINT('Ctrl Pts',(-25.1857745113537,26.3289769635747,-64.1437949684118));
#11322=CARTESIAN_POINT('Ctrl Pts',(-25.0500634284825,26.4032527889375,-64.1528154827761));
#11323=CARTESIAN_POINT('Ctrl Pts',(-25.0019717465166,26.4280214651708,-64.1560040533003));
#11324=CARTESIAN_POINT('Ctrl Pts',(-24.9129931351249,26.4710500833843,-64.1619059019375));
#11325=CARTESIAN_POINT('Ctrl Pts',(-24.8723050178916,26.4896907786571,-64.1646055401226));
#11326=CARTESIAN_POINT('Ctrl Pts',(-24.8241976041084,26.5105296258366,-64.1678029390358));
#11327=CARTESIAN_POINT('Ctrl Pts',(-24.8171409190449,26.5135564874198,-64.1682720865791));
#11328=CARTESIAN_POINT('Ctrl Pts',(-24.8070119844279,26.5178583519208,-64.1689456996727));
#11329=CARTESIAN_POINT('Ctrl Pts',(-24.8039484349128,26.5191538787247,-64.1691494654674));
#11330=CARTESIAN_POINT('Ctrl Pts',(-24.797754630989,26.521761844446,-64.1695614927389));
#11331=CARTESIAN_POINT('Ctrl Pts',(-24.7946242982573,26.5230740853622,-64.1697697606314));
#11332=CARTESIAN_POINT('Ctrl Pts',(-24.7885519642523,26.525608346812,-64.17017382755));
#11333=CARTESIAN_POINT('Ctrl Pts',(-24.7856102113238,26.5268309557386,-64.1703696062909));
#11334=CARTESIAN_POINT('Ctrl Pts',(-24.7785985651787,26.529732850239,-64.1708363120416));
#11335=CARTESIAN_POINT('Ctrl Pts',(-24.7745270414497,26.5314081584667,-64.1711073737709));
#11336=CARTESIAN_POINT('Ctrl Pts',(-24.760034381496,26.537336750307,-64.1720724270894));
#11337=CARTESIAN_POINT('Ctrl Pts',(-24.7495945031162,26.541543738448,-64.1727679848753));
#11338=CARTESIAN_POINT('Ctrl Pts',(-24.5954752786078,26.6027130874594,-64.183042285239));
#11339=CARTESIAN_POINT('Ctrl Pts',(-24.4479248691563,26.6493132853519,-64.192971663129));
#11340=CARTESIAN_POINT('Ctrl Pts',(-24.1397474168328,26.7227836351276,-64.2139015556458));
#11341=CARTESIAN_POINT('Ctrl Pts',(-23.9792671244738,26.7484390923787,-64.2249021758243));
#11342=CARTESIAN_POINT('Ctrl Pts',(-23.7969867016134,26.763609909018,-64.2372758869747));
#11343=CARTESIAN_POINT('Ctrl Pts',(-23.7764062803604,26.7651238937147,-64.2386709477898));
#11344=CARTESIAN_POINT('Ctrl Pts',(-23.7312827380956,26.7680079297472,-64.2417238752259));
#11345=CARTESIAN_POINT('Ctrl Pts',(-23.7067354599254,26.7692950683045,-64.2433809154697));
#11346=CARTESIAN_POINT('Ctrl Pts',(-23.595444845031,26.7738545659571,-64.2508710544743));
#11347=CARTESIAN_POINT('Ctrl Pts',(-23.5085998115634,26.7739025566554,-64.2566551702134));
#11348=CARTESIAN_POINT('Ctrl Pts',(-23.3808723154963,26.7688096680634,-64.2649832745104));
#11349=CARTESIAN_POINT('Ctrl Pts',(-23.3399237487836,26.7663933644623,-64.2676258843719));
#11350=CARTESIAN_POINT('Ctrl Pts',(-23.2785097319228,26.7615913623375,-64.2715373330146));
#11351=CARTESIAN_POINT('Ctrl Pts',(-23.2580042662203,26.7597902303192,-64.2728346027502));
#11352=CARTESIAN_POINT('Ctrl Pts',(-23.2334682470377,26.7573979643734,-64.2743752799697));
#11353=CARTESIAN_POINT('Ctrl Pts',(-23.2294203861404,26.7569955591559,-64.2746290770401));
#11354=CARTESIAN_POINT('Ctrl Pts',(-23.2231637280651,26.7563616080116,-64.2750207675545));
#11355=CARTESIAN_POINT('Ctrl Pts',(-23.2209544086028,26.7561354429847,-64.2751589643834));
#11356=CARTESIAN_POINT('Ctrl Pts',(-23.2170753494578,26.7557342967884,-64.2754014024003));
#11357=CARTESIAN_POINT('Ctrl Pts',(-23.2154055194739,26.7555602953197,-64.2755056988807));
#11358=CARTESIAN_POINT('Ctrl Pts',(-23.2115847019372,26.7551591359306,-64.2757441923877));
#11359=CARTESIAN_POINT('Ctrl Pts',(-23.2094338106437,26.7549311177989,-64.2758783397777));
#11360=CARTESIAN_POINT('Ctrl Pts',(-23.203599402602,26.7543066660653,-64.2762419268376));
#11361=CARTESIAN_POINT('Ctrl Pts',(-23.1999163229079,26.753906044331,-64.2764711290104));
#11362=CARTESIAN_POINT('Ctrl Pts',(-23.182558825884,26.751987716497,-64.2775498360929));
#11363=CARTESIAN_POINT('Ctrl Pts',(-23.1688932611161,26.7503887752986,-64.2783948027208));
#11364=CARTESIAN_POINT('Ctrl Pts',(-22.913597109621,26.7188592286028,-64.2941067873799));
#11365=CARTESIAN_POINT('Ctrl Pts',(-22.6760717109806,26.6617229661908,-64.3075303778215));
#11366=CARTESIAN_POINT('Ctrl Pts',(-22.3516685669515,26.5435542909854,-64.3268327551247));
#11367=CARTESIAN_POINT('Ctrl Pts',(-22.2578217065855,26.504246488997,-64.3325345382842));
#11368=CARTESIAN_POINT('Ctrl Pts',(-22.135434649349,26.4460344653975,-64.3402661806216));
#11369=CARTESIAN_POINT('Ctrl Pts',(-22.1051119255198,26.4310216188492,-64.3422066737569));
#11370=CARTESIAN_POINT('Ctrl Pts',(-22.0750359910842,26.4155367620648,-64.3441594845823));
#11371=CARTESIAN_POINT('',(-26.7730019592961,23.5521733105916,-64.1880685683874));
#11372=CARTESIAN_POINT('Ctrl Pts',(-22.0750364910777,26.4155370194908,-64.5943742034087));
#11373=CARTESIAN_POINT('Ctrl Pts',(-22.1780646657283,26.4685819497682,-64.5877918196014));
#11374=CARTESIAN_POINT('Ctrl Pts',(-22.2839391375605,26.5160625361067,-64.5810957300875));
#11375=CARTESIAN_POINT('Ctrl Pts',(-22.3983059545719,26.5600995864398,-64.5738161306072));
#11376=CARTESIAN_POINT('Ctrl Pts',(-22.4044073340023,26.5624276579996,-64.573427647464));
#11377=CARTESIAN_POINT('Ctrl Pts',(-22.4157079779317,26.5667002821916,-64.5727078670987));
#11378=CARTESIAN_POINT('Ctrl Pts',(-22.4209052800273,26.5686499807631,-64.5723767327745));
#11379=CARTESIAN_POINT('Ctrl Pts',(-22.427897220166,26.5712523270788,-64.571931113021));
#11380=CARTESIAN_POINT('Ctrl Pts',(-22.4296874592215,26.5719168292892,-64.5718170024157));
#11381=CARTESIAN_POINT('Ctrl Pts',(-22.4378856077802,26.5749515362713,-64.5712943893195));
#11382=CARTESIAN_POINT('Ctrl Pts',(-22.444300419849,26.5773029387656,-64.5708852931883));
#11383=CARTESIAN_POINT('Ctrl Pts',(-22.4567063676291,26.5818057427713,-64.5700937691596));
#11384=CARTESIAN_POINT('Ctrl Pts',(-22.4626965001124,26.5839598283584,-64.5697114292238));
#11385=CARTESIAN_POINT('Ctrl Pts',(-22.49506883275,26.5954929016213,-64.5676442442464));
#11386=CARTESIAN_POINT('Ctrl Pts',(-22.5215653955865,26.6045452892871,-64.5659489773829));
#11387=CARTESIAN_POINT('Ctrl Pts',(-22.5553300575076,26.615591581873,-64.563783405865));
#11388=CARTESIAN_POINT('Ctrl Pts',(-22.562492324645,26.617907009312,-64.5633237391642));
#11389=CARTESIAN_POINT('Ctrl Pts',(-22.573911822327,26.6215545812972,-64.5625903487252));
#11390=CARTESIAN_POINT('Ctrl Pts',(-22.5781638506545,26.6229030254114,-64.5623171622451));
#11391=CARTESIAN_POINT('Ctrl Pts',(-22.5856601236553,26.6252631979477,-64.5618353391164));
#11392=CARTESIAN_POINT('Ctrl Pts',(-22.5889032016043,26.6262786331138,-64.5616268247688));
#11393=CARTESIAN_POINT('Ctrl Pts',(-22.5951389192696,26.628220264406,-64.561225769946));
#11394=CARTESIAN_POINT('Ctrl Pts',(-22.5981313166868,26.6291472307829,-64.5610332550633));
#11395=CARTESIAN_POINT('Ctrl Pts',(-22.6059911447151,26.6315694454926,-64.5605274445954));
#11396=CARTESIAN_POINT('Ctrl Pts',(-22.6108607616456,26.6330575193781,-64.5602139138593));
#11397=CARTESIAN_POINT('Ctrl Pts',(-22.6285507061487,26.6384174657231,-64.5590743796717));
#11398=CARTESIAN_POINT('Ctrl Pts',(-22.6413914732721,26.6422209149028,-64.5582461376998));
#11399=CARTESIAN_POINT('Ctrl Pts',(-22.6726781065922,26.6512763171637,-64.5562253475893));
#11400=CARTESIAN_POINT('Ctrl Pts',(-22.6911476935113,26.6564438073532,-64.5550300698933));
#11401=CARTESIAN_POINT('Ctrl Pts',(-22.7603164597583,26.6751320087141,-64.5505444757247));
#11402=CARTESIAN_POINT('Ctrl Pts',(-22.8112950505543,26.6875781548456,-64.5472198126345));
#11403=CARTESIAN_POINT('Ctrl Pts',(-22.9788697514073,26.7241798252357,-64.5362256255348));
#11404=CARTESIAN_POINT('Ctrl Pts',(-23.09649368909,26.7431180920163,-64.528401711457));
#11405=CARTESIAN_POINT('Ctrl Pts',(-23.5145610656521,26.7868606978103,-64.5003235005832));
#11406=CARTESIAN_POINT('Ctrl Pts',(-23.8171464286231,26.7760360307752,-64.4793710460604));
#11407=CARTESIAN_POINT('Ctrl Pts',(-24.1297921637471,26.7205071603411,-64.4592750637541));
#11408=CARTESIAN_POINT('Ctrl Pts',(-24.145739316751,26.7175504511665,-64.458254831787));
#11409=CARTESIAN_POINT('Ctrl Pts',(-24.1651857145036,26.7137928917528,-64.4570171756147));
#11410=CARTESIAN_POINT('Ctrl Pts',(-24.1687064486964,26.7131064932127,-64.4567933587123));
#11411=CARTESIAN_POINT('Ctrl Pts',(-24.1745078341283,26.7119654041509,-64.4564249928107));
#11412=CARTESIAN_POINT('Ctrl Pts',(-24.1767891394709,26.7115141231577,-64.4562802494256));
#11413=CARTESIAN_POINT('Ctrl Pts',(-24.1809011110833,26.7106960793037,-64.4560195569655));
#11414=CARTESIAN_POINT('Ctrl Pts',(-24.182731942712,26.710330195773,-64.4559035576588));
#11415=CARTESIAN_POINT('Ctrl Pts',(-24.1866677232706,26.7095400901692,-64.4556543475747));
#11416=CARTESIAN_POINT('Ctrl Pts',(-24.1887725606375,26.7091153564948,-64.4555211670015));
#11417=CARTESIAN_POINT('Ctrl Pts',(-24.1945347602722,26.7079466115926,-64.4551568306267));
#11418=CARTESIAN_POINT('Ctrl Pts',(-24.1981912716282,26.7071983471801,-64.454925919522));
#11419=CARTESIAN_POINT('Ctrl Pts',(-24.217157503107,26.7032827789512,-64.4537296317806));
#11420=CARTESIAN_POINT('Ctrl Pts',(-24.2324456712568,26.7000103834488,-64.4527702153299));
#11421=CARTESIAN_POINT('Ctrl Pts',(-24.3810285697346,26.6670739901047,-64.4434880310266));
#11422=CARTESIAN_POINT('Ctrl Pts',(-24.5123526628997,26.6290734043046,-64.4356129942025));
#11423=CARTESIAN_POINT('Ctrl Pts',(-24.749909048627,26.5436395086538,-64.4213287727328));
#11424=CARTESIAN_POINT('Ctrl Pts',(-24.8567423901237,26.4985786292396,-64.4148886623379));
#11425=CARTESIAN_POINT('Ctrl Pts',(-25.0186296967779,26.4197657266678,-64.4048138697507));
#11426=CARTESIAN_POINT('Ctrl Pts',(-25.075487202531,26.3899525833706,-64.4012120710736));
#11427=CARTESIAN_POINT('Ctrl Pts',(-25.2185705374298,26.309389483884,-64.3919163838454));
#11428=CARTESIAN_POINT('Ctrl Pts',(-25.3033879943403,26.2562893892899,-64.3861810027071));
#11429=CARTESIAN_POINT('Ctrl Pts',(-25.398408001405,26.1904574282723,-64.379399861288));
#11430=CARTESIAN_POINT('Ctrl Pts',(-25.4111562014552,26.1814876136609,-64.3784824213674));
#11431=CARTESIAN_POINT('Ctrl Pts',(-25.4279939483844,26.1694567650092,-64.3772601518843));
#11432=CARTESIAN_POINT('Ctrl Pts',(-25.4321421373304,26.1664778957545,-64.3769581756646));
#11433=CARTESIAN_POINT('Ctrl Pts',(-25.4395092932312,26.1611608564406,-64.3764203310538));
#11434=CARTESIAN_POINT('Ctrl Pts',(-25.4427310502689,26.1588265574366,-64.3761845991356));
#11435=CARTESIAN_POINT('Ctrl Pts',(-25.4546079283243,26.150187674129,-64.3753136287829));
#11436=CARTESIAN_POINT('Ctrl Pts',(-25.4632358690446,26.1438459787512,-64.374677073599));
#11437=CARTESIAN_POINT('Ctrl Pts',(-25.4750117129926,26.1350997892198,-64.3738029028046));
#11438=CARTESIAN_POINT('Ctrl Pts',(-25.4781870879252,26.13273226974,-64.3735666430997));
#11439=CARTESIAN_POINT('Ctrl Pts',(-25.4867013526749,26.1263596860219,-64.3729316947079));
#11440=CARTESIAN_POINT('Ctrl Pts',(-25.4920321593862,26.12234389542,-64.3725326103673));
#11441=CARTESIAN_POINT('Ctrl Pts',(-25.5013500907741,26.1152790561357,-64.3718323026586));
#11442=CARTESIAN_POINT('Ctrl Pts',(-25.5053426505667,26.112237188713,-64.3715313498147));
#11443=CARTESIAN_POINT('Ctrl Pts',(-25.5188891430615,26.1018662266614,-64.3705072061383));
#11444=CARTESIAN_POINT('Ctrl Pts',(-25.5284090163246,26.0944929826612,-64.3697823425302));
#11445=CARTESIAN_POINT('Ctrl Pts',(-25.5562851608059,26.0726515743902,-64.367644379668));
#11446=CARTESIAN_POINT('Ctrl Pts',(-25.5745253250545,26.0580371024075,-64.3662256107699));
#11447=CARTESIAN_POINT('Ctrl Pts',(-25.5976444672417,26.0390968967569,-64.3644011194768));
#11448=CARTESIAN_POINT('Ctrl Pts',(-25.60267182314,26.0349527273649,-64.3640027688925));
#11449=CARTESIAN_POINT('Ctrl Pts',(-25.610653082668,26.0283328343849,-64.3633677816671));
#11450=CARTESIAN_POINT('Ctrl Pts',(-25.613615189994,26.0258669922203,-64.3631315485092));
#11451=CARTESIAN_POINT('Ctrl Pts',(-25.6191333424658,26.0212565555665,-64.3626904005233));
#11452=CARTESIAN_POINT('Ctrl Pts',(-25.6216904967599,26.0191132916244,-64.3624855403691));
#11453=CARTESIAN_POINT('Ctrl Pts',(-25.626699215275,26.0149020036599,-64.3620834348067));
#11454=CARTESIAN_POINT('Ctrl Pts',(-25.6291510303761,26.0128342829208,-64.361886202002));
#11455=CARTESIAN_POINT('Ctrl Pts',(-25.636545993412,26.0065788792235,-64.3612901171786));
#11456=CARTESIAN_POINT('Ctrl Pts',(-25.6414795823003,26.0023799663527,-64.3608908025617));
#11457=CARTESIAN_POINT('Ctrl Pts',(-25.6657977429401,25.9815563311956,-64.3589144085593));
#11458=CARTESIAN_POINT('Ctrl Pts',(-25.6849964604655,25.9647168624245,-64.3573284393562));
#11459=CARTESIAN_POINT('Ctrl Pts',(-25.7366662393825,25.9182985235305,-64.3529885504479));
#11460=CARTESIAN_POINT('Ctrl Pts',(-25.7687350277746,25.8882820073453,-64.350216288159));
#11461=CARTESIAN_POINT('Ctrl Pts',(-25.8562926991825,25.8029040677121,-64.3424208715681));
#11462=CARTESIAN_POINT('Ctrl Pts',(-25.9103875456094,25.7461626638787,-64.3373400830642));
#11463=CARTESIAN_POINT('Ctrl Pts',(-26.0715152812713,25.5643141749668,-64.3213657804476));
#11464=CARTESIAN_POINT('Ctrl Pts',(-26.1710664721605,25.4329463392836,-64.3102370109255));
#11465=CARTESIAN_POINT('Ctrl Pts',(-26.3499348240832,25.1550639360616,-64.2878690354011));
#11466=CARTESIAN_POINT('Ctrl Pts',(-26.4288313082328,25.0088255016172,-64.2766650016213));
#11467=CARTESIAN_POINT('Ctrl Pts',(-26.5115508950291,24.8223678775062,-64.2635420867628));
#11468=CARTESIAN_POINT('Ctrl Pts',(-26.5263651183379,24.7873134190912,-64.2611235630608));
#11469=CARTESIAN_POINT('Ctrl Pts',(-26.5425141385358,24.7471299772286,-64.2584127964122));
#11470=CARTESIAN_POINT('Ctrl Pts',(-26.5444605980969,24.7422521958828,-64.2580847664786));
#11471=CARTESIAN_POINT('Ctrl Pts',(-26.5472928226342,24.7351039974642,-64.2576055726203));
#11472=CARTESIAN_POINT('Ctrl Pts',(-26.5481879369135,24.7328373310562,-64.2574538455939));
#11473=CARTESIAN_POINT('Ctrl Pts',(-26.5497706101838,24.728816238083,-64.2571850790434));
#11474=CARTESIAN_POINT('Ctrl Pts',(-26.5504592018574,24.7270622230143,-64.2570679766538));
#11475=CARTESIAN_POINT('Ctrl Pts',(-26.5518965742178,24.7233914148583,-64.2568231867984));
#11476=CARTESIAN_POINT('Ctrl Pts',(-26.5526450558276,24.7214745124877,-64.2566955177541));
#11477=CARTESIAN_POINT('Ctrl Pts',(-26.5546007548049,24.7164516660621,-64.2563614047447));
#11478=CARTESIAN_POINT('Ctrl Pts',(-26.555804995818,24.7133445539983,-64.2561551414442));
#11479=CARTESIAN_POINT('Ctrl Pts',(-26.5610685554054,24.6997010632646,-64.2552512368258));
#11480=CARTESIAN_POINT('Ctrl Pts',(-26.5650773687746,24.6891450929245,-64.2545566137816));
#11481=CARTESIAN_POINT('Ctrl Pts',(-26.5940491188967,24.6116319486059,-64.2494890156958));
#11482=CARTESIAN_POINT('Ctrl Pts',(-26.6168365543966,24.5438762741761,-64.2452395640017));
#11483=CARTESIAN_POINT('Ctrl Pts',(-26.7271183623599,24.1758849465667,-64.2228374271424));
#11484=CARTESIAN_POINT('Ctrl Pts',(-26.7728155786524,23.8648892164005,-64.2061317082339));
#11485=CARTESIAN_POINT('Ctrl Pts',(-26.7730019592961,23.5521733105916,-64.1880685683874));
#11486=CARTESIAN_POINT('Ctrl Pts',(-26.7730019617299,23.5521692227448,-64.1880683322646));
#11487=CARTESIAN_POINT('Ctrl Pts',(-26.7730705287399,23.4368797543027,-64.1814089624338));
#11488=CARTESIAN_POINT('Ctrl Pts',(-26.7669527001803,23.3216786349966,-64.1746044679484));
#11489=CARTESIAN_POINT('Ctrl Pts',(-26.7537718069693,23.1986077503722,-64.1670816578786));
#11490=CARTESIAN_POINT('Ctrl Pts',(-26.7528332958108,23.190160534511,-64.1665640493305));
#11491=CARTESIAN_POINT('Ctrl Pts',(-26.7512863760238,23.1767218447392,-64.1657385339867));
#11492=CARTESIAN_POINT('Ctrl Pts',(-26.7506996767062,23.1717278717666,-64.1654313116746));
#11493=CARTESIAN_POINT('Ctrl Pts',(-26.7496753844482,23.1631817617928,-64.1649047866224));
#11494=CARTESIAN_POINT('Ctrl Pts',(-26.7492435562446,23.1596289324079,-64.1646856661647));
#11495=CARTESIAN_POINT('Ctrl Pts',(-26.7484226643033,23.1529677742654,-64.1642744037089));
#11496=CARTESIAN_POINT('Ctrl Pts',(-26.7480349846954,23.1498592765489,-64.1640823056801));
#11497=CARTESIAN_POINT('Ctrl Pts',(-26.7472190114404,23.1433934095522,-64.1636823570839));
#11498=CARTESIAN_POINT('Ctrl Pts',(-26.7467899600381,23.1400361412994,-64.1634744827644));
#11499=CARTESIAN_POINT('Ctrl Pts',(-26.7457940840224,23.1323399844659,-64.1629974717991));
#11500=CARTESIAN_POINT('Ctrl Pts',(-26.7452237105887,23.1280015689735,-64.1627282230921));
#11501=CARTESIAN_POINT('Ctrl Pts',(-26.7433975020945,23.1143264932296,-64.1618784091012));
#11502=CARTESIAN_POINT('Ctrl Pts',(-26.7421095708715,23.1049942342591,-64.1612968279706));
#11503=CARTESIAN_POINT('Ctrl Pts',(-26.7311149402433,23.0278278017878,-64.1564740561185));
#11504=CARTESIAN_POINT('Ctrl Pts',(-26.7192885460338,22.9603179288108,-64.1521659018376));
#11505=CARTESIAN_POINT('Ctrl Pts',(-26.7029014511981,22.8816247409082,-64.1470334688314));
#11506=CARTESIAN_POINT('Ctrl Pts',(-26.700418542194,22.8700228405997,-64.1462739551814));
#11507=CARTESIAN_POINT('Ctrl Pts',(-26.6922833644443,22.8330095514438,-64.1438418371539));
#11508=CARTESIAN_POINT('Ctrl Pts',(-26.6863873435955,22.8076532936505,-64.1421620155736));
#11509=CARTESIAN_POINT('Ctrl Pts',(-26.6756982682776,22.7640839196378,-64.1392520669069));
#11510=CARTESIAN_POINT('Ctrl Pts',(-26.6710514943295,22.7458360026547,-64.1380261469508));
#11511=CARTESIAN_POINT('Ctrl Pts',(-26.5869685102774,22.4273399880419,-64.116504830388));
#11512=CARTESIAN_POINT('Ctrl Pts',(-26.4647201024252,22.1401423477394,-64.0949388877303));
#11513=CARTESIAN_POINT('Ctrl Pts',(-26.2760375579856,21.8300885540783,-64.0710959493273));
#11514=CARTESIAN_POINT('Ctrl Pts',(-26.2476820355212,21.7859558206728,-64.0676931377554));
#11515=CARTESIAN_POINT('Ctrl Pts',(-26.2041085302775,21.7216458453609,-64.0627429431857));
#11516=CARTESIAN_POINT('Ctrl Pts',(-26.1897115346993,21.7009255345114,-64.0611493645717));
#11517=CARTESIAN_POINT('Ctrl Pts',(-26.1725719836609,21.676866073317,-64.0593025944261));
#11518=CARTESIAN_POINT('Ctrl Pts',(-26.1700647569084,21.6733614757914,-64.059033677503));
#11519=CARTESIAN_POINT('Ctrl Pts',(-26.1662244272954,21.668016157295,-64.0586236698543));
#11520=CARTESIAN_POINT('Ctrl Pts',(-26.1648964063172,21.6661718177491,-64.0584822293488));
#11521=CARTESIAN_POINT('Ctrl Pts',(-26.1624858797467,21.662831564512,-64.0582261215776));
#11522=CARTESIAN_POINT('Ctrl Pts',(-26.1614040434038,21.6613351817333,-64.0581114086065));
#11523=CARTESIAN_POINT('Ctrl Pts',(-26.1590409811853,21.658072532469,-64.0578613358065));
#11524=CARTESIAN_POINT('Ctrl Pts',(-26.1577592507941,21.6563066418698,-64.0577260122036));
#11525=CARTESIAN_POINT('Ctrl Pts',(-26.1542483825853,21.6514798994808,-64.0573561991558));
#11526=CARTESIAN_POINT('Ctrl Pts',(-26.1520156332272,21.6484216600992,-64.057121961034));
#11527=CARTESIAN_POINT('Ctrl Pts',(-26.1411581357811,21.6336048429315,-64.0559874385039));
#11528=CARTESIAN_POINT('Ctrl Pts',(-26.1324588573702,21.6219007166078,-64.0550922774014));
#11529=CARTESIAN_POINT('Ctrl Pts',(-26.1183830893925,21.6032290506122,-64.0536651532135));
#11530=CARTESIAN_POINT('Ctrl Pts',(-26.1130571136743,21.5962239557053,-64.0531299482134));
#11531=CARTESIAN_POINT('Ctrl Pts',(-26.1045092496733,21.5850762749948,-64.0522784242872));
#11532=CARTESIAN_POINT('Ctrl Pts',(-26.1013058642982,21.580919650687,-64.0519609585373));
#11533=CARTESIAN_POINT('Ctrl Pts',(-26.0953314460543,21.5732064499163,-64.0513718941258));
#11534=CARTESIAN_POINT('Ctrl Pts',(-26.0925630806866,21.5696478354548,-64.051100134468));
#11535=CARTESIAN_POINT('Ctrl Pts',(-25.8970870582046,21.3194569403249,-64.0319940167032));
#11536=CARTESIAN_POINT('Ctrl Pts',(-25.6694571300877,21.1021675974939,-64.0152769791579));
#11537=CARTESIAN_POINT('Ctrl Pts',(-25.3563507809447,20.8802103790905,-63.9934677852187));
#11538=CARTESIAN_POINT('Ctrl Pts',(-25.2973460683086,20.8412343809095,-63.9894094864369));
#11539=CARTESIAN_POINT('Ctrl Pts',(-25.1806798013622,20.7695672835645,-63.9814302668747));
#11540=CARTESIAN_POINT('Ctrl Pts',(-25.1231978877306,20.7366524274511,-63.9775188885714));
#11541=CARTESIAN_POINT('Ctrl Pts',(-25.0340302718407,20.6891807018647,-63.9714562613091));
#11542=CARTESIAN_POINT('Ctrl Pts',(-25.0030530761247,20.6733272928093,-63.9693510342015));
#11543=CARTESIAN_POINT('Ctrl Pts',(-24.9654104574199,20.6548256697856,-63.9667918701821));
#11544=CARTESIAN_POINT('Ctrl Pts',(-24.9589843242541,20.6516936824145,-63.9663549528071));
#11545=CARTESIAN_POINT('Ctrl Pts',(-24.9496022686101,20.6471595984169,-63.965716995902));
#11546=CARTESIAN_POINT('Ctrl Pts',(-24.9466545159541,20.6457405651702,-63.9655165467038));
#11547=CARTESIAN_POINT('Ctrl Pts',(-24.9407857025368,20.6429263473029,-63.9651174427771));
#11548=CARTESIAN_POINT('Ctrl Pts',(-24.9378646900798,20.6415310703925,-63.9649187915497));
#11549=CARTESIAN_POINT('Ctrl Pts',(-24.9320349983477,20.6387571876583,-63.9645223054992));
#11550=CARTESIAN_POINT('Ctrl Pts',(-24.9291263457955,20.6373785337065,-63.9643244726193));
#11551=CARTESIAN_POINT('Ctrl Pts',(-24.9221225438031,20.6340716867194,-63.9638480778172));
#11552=CARTESIAN_POINT('Ctrl Pts',(-24.9180253959663,20.6321477628146,-63.9635693681469));
#11553=CARTESIAN_POINT('Ctrl Pts',(-24.9054503450736,20.6262751178796,-63.9627138650032));
#11554=CARTESIAN_POINT('Ctrl Pts',(-24.8969593519087,20.6223546906975,-63.9621360938527));
#11555=CARTESIAN_POINT('Ctrl Pts',(-24.798450267718,20.5773906420531,-63.9554314511367));
#11556=CARTESIAN_POINT('Ctrl Pts',(-24.706614192966,20.5404801744819,-63.9491632588301));
#11557=CARTESIAN_POINT('Ctrl Pts',(-24.4515056107939,20.4513479872491,-63.9316767772493));
#11558=CARTESIAN_POINT('Ctrl Pts',(-24.2855480110023,20.4078339992852,-63.920206275327));
#11559=CARTESIAN_POINT('Ctrl Pts',(-24.0984010274011,20.3744053370231,-63.9073502830479));
#11560=CARTESIAN_POINT('Ctrl Pts',(-24.0798345943667,20.371256618963,-63.9060759795227));
#11561=CARTESIAN_POINT('Ctrl Pts',(-24.0400091674661,20.364861120029,-63.9033458209433));
#11562=CARTESIAN_POINT('Ctrl Pts',(-24.0187430595912,20.3616640299179,-63.9018899381512));
#11563=CARTESIAN_POINT('Ctrl Pts',(-23.9726839482421,20.3552103589659,-63.8987424266396));
#11564=CARTESIAN_POINT('Ctrl Pts',(-23.9478817041959,20.3520289874423,-63.8970510918087));
#11565=CARTESIAN_POINT('Ctrl Pts',(-23.7509057044796,20.3290897560119,-63.8836560086442));
#11566=CARTESIAN_POINT('Ctrl Pts',(-23.5774040922814,20.3229578260456,-63.8720677024364));
#11567=CARTESIAN_POINT('Ctrl Pts',(-23.3981300478816,20.3310890370325,-63.8608231382064));
#11568=CARTESIAN_POINT('Ctrl Pts',(-23.3920302638334,20.3313830763026,-63.8604414352876));
#11569=CARTESIAN_POINT('Ctrl Pts',(-23.3833141402341,20.3318280719158,-63.8598973222624));
#11570=CARTESIAN_POINT('Ctrl Pts',(-23.3806971400581,20.3319648815412,-63.8597341222876));
#11571=CARTESIAN_POINT('Ctrl Pts',(-23.3761756236782,20.3322067845418,-63.8594524492695));
#11572=CARTESIAN_POINT('Ctrl Pts',(-23.3742710313197,20.3323103767962,-63.8593338911152));
#11573=CARTESIAN_POINT('Ctrl Pts',(-23.3706065260107,20.3325129551915,-63.8591059565364));
#11574=CARTESIAN_POINT('Ctrl Pts',(-23.3688466057643,20.33261169412,-63.8589965661811));
#11575=CARTESIAN_POINT('Ctrl Pts',(-23.3646788386604,20.3328489536766,-63.8587376950889));
#11576=CARTESIAN_POINT('Ctrl Pts',(-23.3622710604257,20.3329887336921,-63.8585882857958));
#11577=CARTESIAN_POINT('Ctrl Pts',(-23.3550937191874,20.3334134884345,-63.8581433358596));
#11578=CARTESIAN_POINT('Ctrl Pts',(-23.3503246035648,20.3337063690241,-63.8578482388794));
#11579=CARTESIAN_POINT('Ctrl Pts',(-23.306162805618,20.3365170280623,-63.8551206783509));
#11580=CARTESIAN_POINT('Ctrl Pts',(-23.2668166795536,20.3397478758041,-63.8527275748206));
#11581=CARTESIAN_POINT('Ctrl Pts',(-22.9865928048519,20.367950260551,-63.8358852588362));
#11582=CARTESIAN_POINT('Ctrl Pts',(-22.7491153052075,20.4192827474275,-63.8226332760825));
#11583=CARTESIAN_POINT('Ctrl Pts',(-22.4165045867567,20.5315484604748,-63.8029538420744));
#11584=CARTESIAN_POINT('Ctrl Pts',(-22.3152359230958,20.5715463418504,-63.7968083420412));
#11585=CARTESIAN_POINT('Ctrl Pts',(-22.1427337938606,20.6499904795538,-63.7858679392452));
#11586=CARTESIAN_POINT('Ctrl Pts',(-22.0705641230587,20.6861384169175,-63.7811390921964));
#11587=CARTESIAN_POINT('Ctrl Pts',(-21.9749264968325,20.7386208981422,-63.7746199851272));
#11588=CARTESIAN_POINT('Ctrl Pts',(-21.9502046603625,20.7526157985357,-63.772911320248));
#11589=CARTESIAN_POINT('Ctrl Pts',(-21.9151779193311,20.7730603869728,-63.7704551427186));
#11590=CARTESIAN_POINT('Ctrl Pts',(-21.9047190337172,20.7792446469253,-63.7697171814));
#11591=CARTESIAN_POINT('Ctrl Pts',(-21.8887288906729,20.7888219502665,-63.7685818289633));
#11592=CARTESIAN_POINT('Ctrl Pts',(-21.8831724155348,20.7921728462872,-63.7681859739347));
#11593=CARTESIAN_POINT('Ctrl Pts',(-21.8728787535881,20.7984230279495,-63.7674501460662));
#11594=CARTESIAN_POINT('Ctrl Pts',(-21.8681388605158,20.8013178278895,-63.7671103384819));
#11595=CARTESIAN_POINT('Ctrl Pts',(-21.8603629806659,20.806094441098,-63.7665512507349));
#11596=CARTESIAN_POINT('Ctrl Pts',(-21.8573225839227,20.8079690830634,-63.7663322351592));
#11597=CARTESIAN_POINT('Ctrl Pts',(-21.8514058872887,20.811630778334,-63.7659052218427));
#11598=CARTESIAN_POINT('Ctrl Pts',(-21.8485292740805,20.8134173186164,-63.7656972432565));
#11599=CARTESIAN_POINT('Ctrl Pts',(-21.8419328394238,20.8175285001512,-63.7652194674915));
#11600=CARTESIAN_POINT('Ctrl Pts',(-21.8382149437047,20.8198562050452,-63.7649495570465));
#11601=CARTESIAN_POINT('Ctrl Pts',(-21.82647934245,20.8272370391897,-63.7640955926265));
#11602=CARTESIAN_POINT('Ctrl Pts',(-21.8184792235889,20.8323179138948,-63.7635105085979));
#11603=CARTESIAN_POINT('Ctrl Pts',(-21.7516147202846,20.8751986197399,-63.7585955080922));
#11604=CARTESIAN_POINT('Ctrl Pts',(-21.6939770742644,20.9148680064451,-63.7541957612489));
#11605=CARTESIAN_POINT('Ctrl Pts',(-21.6317022968779,20.9607858485135,-63.7492521478341));
#11606=CARTESIAN_POINT('Ctrl Pts',(-21.625740732974,20.9652134523057,-63.7487769219705));
#11607=CARTESIAN_POINT('Ctrl Pts',(-21.38639132393,21.1442631291757,-63.7296174940043));
#11608=CARTESIAN_POINT('Ctrl Pts',(-21.1777833691933,21.3497046968137,-63.7096775556436));
#11609=CARTESIAN_POINT('Ctrl Pts',(-20.9752499967116,21.6119347115869,-63.6874130259167));
#11610=CARTESIAN_POINT('Ctrl Pts',(-20.9514161569602,21.6440091877463,-63.6847399501044));
#11611=CARTESIAN_POINT('Ctrl Pts',(-20.8852383737793,21.7366171747634,-63.6771791611519));
#11612=CARTESIAN_POINT('Ctrl Pts',(-20.844367722759,21.7981786775426,-63.6723387859319));
#11613=CARTESIAN_POINT('Ctrl Pts',(-20.7897666933114,21.8868964752515,-63.6656757659608));
#11614=CARTESIAN_POINT('Ctrl Pts',(-20.7742511734583,21.9129217593063,-63.6637577115796));
#11615=CARTESIAN_POINT('Ctrl Pts',(-20.7568460347575,21.9430754687577,-63.6615804674114));
#11616=CARTESIAN_POINT('Ctrl Pts',(-20.7545959827465,21.9469925934194,-63.6612984969028));
#11617=CARTESIAN_POINT('Ctrl Pts',(-20.7512045808096,21.952925546657,-63.6608727410235));
#11618=CARTESIAN_POINT('Ctrl Pts',(-20.7500571678572,21.9549378752999,-63.6607285634278));
#11619=CARTESIAN_POINT('Ctrl Pts',(-20.7479891984159,21.9585737774107,-63.6604684781199));
#11620=CARTESIAN_POINT('Ctrl Pts',(-20.7470678850446,21.9601969091706,-63.6603525212478));
#11621=CARTESIAN_POINT('Ctrl Pts',(-20.7450863575523,21.9636949571812,-63.6601029429255));
#11622=CARTESIAN_POINT('Ctrl Pts',(-20.7440266158362,21.9655701310136,-63.6599693525064));
#11623=CARTESIAN_POINT('Ctrl Pts',(-20.7411683870409,21.9706395195118,-63.6596087352707));
#11624=CARTESIAN_POINT('Ctrl Pts',(-20.7393734617399,21.9738357548205,-63.6593819394515));
#11625=CARTESIAN_POINT('Ctrl Pts',(-20.7310542713298,21.9887091755037,-63.6583291888951));
#11626=CARTESIAN_POINT('Ctrl Pts',(-20.7245971693526,22.0004240661892,-63.657507512998));
#11627=CARTESIAN_POINT('Ctrl Pts',(-20.6101705098749,22.2111167425203,-63.6428576504378));
#11628=CARTESIAN_POINT('Ctrl Pts',(-20.5233708623193,22.4209211035782,-63.6302824706869));
#11629=CARTESIAN_POINT('Ctrl Pts',(-20.4155552430319,22.786280755243,-63.6089976397962));
#11630=CARTESIAN_POINT('Ctrl Pts',(-20.3825453478305,22.9373846372241,-63.6003619625065));
#11631=CARTESIAN_POINT('Ctrl Pts',(-20.3488509014325,23.1710363277222,-63.5867271118006));
#11632=CARTESIAN_POINT('Ctrl Pts',(-20.340275900134,23.2522160021309,-63.5819414628024));
#11633=CARTESIAN_POINT('Ctrl Pts',(-20.3329668243196,23.3607086887941,-63.5754372235408));
#11634=CARTESIAN_POINT('Ctrl Pts',(-20.3314846938707,23.3878095276511,-63.5738036343527));
#11635=CARTESIAN_POINT('Ctrl Pts',(-20.3298518885951,23.42665965181,-63.5714478470625));
#11636=CARTESIAN_POINT('Ctrl Pts',(-20.3294228661545,23.4383965442188,-63.5707343241441));
#11637=CARTESIAN_POINT('Ctrl Pts',(-20.3287777064455,23.4591540797623,-63.5694690742153));
#11638=CARTESIAN_POINT('Ctrl Pts',(-20.3285352783116,23.4681738237055,-63.5689181744574));
#11639=CARTESIAN_POINT('Ctrl Pts',(-20.3282326278722,23.4815209482628,-63.5681012868246));
#11640=CARTESIAN_POINT('Ctrl Pts',(-20.3281432371977,23.4858476777182,-63.567836215073));
#11641=CARTESIAN_POINT('Ctrl Pts',(-20.3280026692474,23.4933868240555,-63.5673738777901));
#11642=CARTESIAN_POINT('Ctrl Pts',(-20.3279475800626,23.4965991691428,-63.5671767353543));
#11643=CARTESIAN_POINT('Ctrl Pts',(-20.3278474708148,23.5029945197416,-63.5667839588131));
#11644=CARTESIAN_POINT('Ctrl Pts',(-20.3278023630571,23.5061775205948,-63.5665883276749));
#11645=CARTESIAN_POINT('Ctrl Pts',(-20.3277062275509,23.5137534786727,-63.5661223546301));
#11646=CARTESIAN_POINT('Ctrl Pts',(-20.3276594664604,23.5181464757379,-63.5658518789999));
#11647=CARTESIAN_POINT('Ctrl Pts',(-20.3275253910226,23.5337375606902,-63.5648909503702));
#11648=CARTESIAN_POINT('Ctrl Pts',(-20.3274874617954,23.5449358939998,-63.5641989487157));
#11649=CARTESIAN_POINT('Ctrl Pts',(-20.3277827164481,23.7067180442737,-63.5541748757634));
#11650=CARTESIAN_POINT('Ctrl Pts',(-20.3386109575935,23.8570743859712,-63.5445104736917));
#11651=CARTESIAN_POINT('Ctrl Pts',(-20.383242116857,24.1694315288084,-63.5236926312479));
#11652=CARTESIAN_POINT('Ctrl Pts',(-20.4190849993574,24.3307138271311,-63.5125132354459));
#11653=CARTESIAN_POINT('Ctrl Pts',(-20.5209831463022,24.6655470477836,-63.4888345211913));
#11654=CARTESIAN_POINT('Ctrl Pts',(-20.5900065332292,24.8376204989938,-63.4763831031391));
#11655=CARTESIAN_POINT('Ctrl Pts',(-20.6785543885421,25.0129885654721,-63.464006812399));
#11656=CARTESIAN_POINT('Ctrl Pts',(-20.6837347623607,25.0231146492112,-63.4632934129737));
#11657=CARTESIAN_POINT('Ctrl Pts',(-20.6905061934833,25.0361797194081,-63.4623747614039));
#11658=CARTESIAN_POINT('Ctrl Pts',(-20.6920482787161,25.0391437885016,-63.46216646784));
#11659=CARTESIAN_POINT('Ctrl Pts',(-20.6945485030537,25.0439313145061,-63.4618302366219));
#11660=CARTESIAN_POINT('Ctrl Pts',(-20.6955037805067,25.045756250535,-63.4617021176151));
#11661=CARTESIAN_POINT('Ctrl Pts',(-20.6973360154508,25.0492483496673,-63.4614570488109));
#11662=CARTESIAN_POINT('Ctrl Pts',(-20.6982126822449,25.0509156544913,-63.4613400813654));
#11663=CARTESIAN_POINT('Ctrl Pts',(-20.7002249508003,25.0547345919815,-63.461072261053));
#11664=CARTESIAN_POINT('Ctrl Pts',(-20.7013615300407,25.0568857127884,-63.4609214707655));
#11665=CARTESIAN_POINT('Ctrl Pts',(-20.7049491906215,25.0636572414902,-63.4604470009825));
#11666=CARTESIAN_POINT('Ctrl Pts',(-20.7074091004057,25.0682730007409,-63.4601238819635));
#11667=CARTESIAN_POINT('Ctrl Pts',(-20.7276044065669,25.1059460913777,-63.4574889190918));
#11668=CARTESIAN_POINT('Ctrl Pts',(-20.7459054601704,25.1386991601131,-63.4552124639472));
#11669=CARTESIAN_POINT('Ctrl Pts',(-20.7685316002909,25.1775822475626,-63.4525182583337));
#11670=CARTESIAN_POINT('Ctrl Pts',(-20.7723104414398,25.1840245750366,-63.4520721474949));
#11671=CARTESIAN_POINT('Ctrl Pts',(-20.7777491995604,25.193223373798,-63.4514354721573));
#11672=CARTESIAN_POINT('Ctrl Pts',(-20.779390873138,25.1959905375744,-63.4512439893964));
#11673=CARTESIAN_POINT('Ctrl Pts',(-20.9230350018789,25.437289258005,-63.4345496835121));
#11674=CARTESIAN_POINT('Ctrl Pts',(-21.0952746094889,25.656506257936,-63.419566435846));
#11675=CARTESIAN_POINT('Ctrl Pts',(-21.4236109891949,25.9785704188034,-63.3935584218942));
#11676=CARTESIAN_POINT('Ctrl Pts',(-21.5642871937126,26.094905502202,-63.3830085985986));
#11677=CARTESIAN_POINT('Ctrl Pts',(-21.720765885027,26.2033947132951,-63.3714322668509));
#11678=CARTESIAN_POINT('Ctrl Pts',(-21.7275236265351,26.2080418691839,-63.3709326720764));
#11679=CARTESIAN_POINT('Ctrl Pts',(-21.7383512948461,26.2154271096762,-63.3701327074382));
#11680=CARTESIAN_POINT('Ctrl Pts',(-21.7424098921548,26.2181818061423,-63.3698329674857));
#11681=CARTESIAN_POINT('Ctrl Pts',(-21.750146871013,26.2234073735587,-63.3692617791981));
#11682=CARTESIAN_POINT('Ctrl Pts',(-21.7538240936852,26.2258799469002,-63.3689903960166));
#11683=CARTESIAN_POINT('Ctrl Pts',(-21.7602778753613,26.2302001832959,-63.3685142530566));
#11684=CARTESIAN_POINT('Ctrl Pts',(-21.7630522309862,26.2320511390944,-63.3683096179469));
#11685=CARTESIAN_POINT('Ctrl Pts',(-21.7684700755802,26.2356535999541,-63.3679100945696));
#11686=CARTESIAN_POINT('Ctrl Pts',(-21.7711132872709,26.2374055171343,-63.3677152221218));
#11687=CARTESIAN_POINT('Ctrl Pts',(-21.7773855351155,26.2415494433325,-63.367252897615));
#11688=CARTESIAN_POINT('Ctrl Pts',(-21.7810168267222,26.2439380133561,-63.3669853166727));
#11689=CARTESIAN_POINT('Ctrl Pts',(-21.793790316946,26.252303114041,-63.3660443412977));
#11690=CARTESIAN_POINT('Ctrl Pts',(-21.8029579781024,26.2582404562732,-63.3653694813257));
#11691=CARTESIAN_POINT('Ctrl Pts',(-21.8973802780614,26.3187129920576,-63.358423383883));
#11692=CARTESIAN_POINT('Ctrl Pts',(-21.9851050021773,26.3692350120708,-63.3520057379053));
#11693=CARTESIAN_POINT('Ctrl Pts',(-22.0750360636209,26.415536799411,-63.3454515897691));
#11694=CARTESIAN_POINT('Origin',(-23.5502525316942,23.5502525316942,-77.3107734492734));
#11695=CARTESIAN_POINT('',(-22.0750358661665,26.4155366977499,-61.8467738923868));
#11696=CARTESIAN_POINT('',(-22.0750361387181,26.4155368380754,-62.0907209741597));
#11697=CARTESIAN_POINT('',(-22.0750360153461,26.4155367745563,-77.3107734492734));
#11698=CARTESIAN_POINT('Ctrl Pts',(-22.0750358661665,26.4155366977499,-61.8467738923868));
#11699=CARTESIAN_POINT('Ctrl Pts',(-22.0129928290477,26.3835932963163,-61.8514971515873));
#11700=CARTESIAN_POINT('Ctrl Pts',(-21.9519838212122,26.3496329512428,-61.8562169656468));
#11701=CARTESIAN_POINT('Ctrl Pts',(-21.8373123293699,26.2808269866894,-61.8651844232319));
#11702=CARTESIAN_POINT('Ctrl Pts',(-21.7835048400784,26.2463245648821,-61.8694349606208));
#11703=CARTESIAN_POINT('Ctrl Pts',(-21.6934078442242,26.1846961059217,-61.8765849758899));
#11704=CARTESIAN_POINT('Ctrl Pts',(-21.6565993848976,26.158363601384,-61.8795157905653));
#11705=CARTESIAN_POINT('Ctrl Pts',(-21.6064397654188,26.1208577951366,-61.8835101114855));
#11706=CARTESIAN_POINT('Ctrl Pts',(-21.5926077685641,26.1103397378112,-61.8846116248033));
#11707=CARTESIAN_POINT('Ctrl Pts',(-21.5703016825142,26.093091352665,-61.8863871260411));
#11708=CARTESIAN_POINT('Ctrl Pts',(-21.5617754331277,26.0864294717038,-61.8870655873375));
#11709=CARTESIAN_POINT('Ctrl Pts',(-21.5513643027722,26.0782100837868,-61.8878936144888));
#11710=CARTESIAN_POINT('Ctrl Pts',(-21.5494475683152,26.076693315785,-61.8880460403279));
#11711=CARTESIAN_POINT('Ctrl Pts',(-21.5457396459331,26.0737522622679,-61.8883408709369));
#11712=CARTESIAN_POINT('Ctrl Pts',(-21.5439482466329,26.0723282472925,-61.8884832948846));
#11713=CARTESIAN_POINT('Ctrl Pts',(-21.5406999781058,26.0697404903059,-61.8887415132444));
#11714=CARTESIAN_POINT('Ctrl Pts',(-21.5392426069797,26.0685773959592,-61.8888573534907));
#11715=CARTESIAN_POINT('Ctrl Pts',(-21.5363096647928,26.0662325127808,-61.8890904558248));
#11716=CARTESIAN_POINT('Ctrl Pts',(-21.5348341301348,26.0650506951802,-61.8892077149119));
#11717=CARTESIAN_POINT('Ctrl Pts',(-21.5306129876552,26.0616637038761,-61.8895431315617));
#11718=CARTESIAN_POINT('Ctrl Pts',(-21.5278699422708,26.0594553186138,-61.8897610571771));
#11719=CARTESIAN_POINT('Ctrl Pts',(-21.5160367778353,26.0498966036187,-61.8907010168086));
#11720=CARTESIAN_POINT('Ctrl Pts',(-21.5069829207361,26.0425012204043,-61.8914198336178));
#11721=CARTESIAN_POINT('Ctrl Pts',(-21.3537252064486,25.915920523576,-61.903585079186));
#11722=CARTESIAN_POINT('Ctrl Pts',(-21.2201044370545,25.7844301338131,-61.9141651539333));
#11723=CARTESIAN_POINT('Ctrl Pts',(-21.0042306133337,25.5314248576174,-61.9327968648602));
#11724=CARTESIAN_POINT('Ctrl Pts',(-20.9174253597454,25.4145195206886,-61.9408650345672));
#11725=CARTESIAN_POINT('Ctrl Pts',(-20.7736815747476,25.1907685421282,-61.9559679589358));
#11726=CARTESIAN_POINT('Ctrl Pts',(-20.714291973527,25.0858183633581,-61.9629291043031));
#11727=CARTESIAN_POINT('Ctrl Pts',(-20.6379033760903,24.9312087942067,-61.9731902315352));
#11728=CARTESIAN_POINT('Ctrl Pts',(-20.6160167922721,24.8840733417468,-61.9763185172515));
#11729=CARTESIAN_POINT('Ctrl Pts',(-20.592103434601,24.8291328396221,-61.9799719750568));
#11730=CARTESIAN_POINT('Ctrl Pts',(-20.5889537600267,24.8218226264068,-61.9804582327944));
#11731=CARTESIAN_POINT('Ctrl Pts',(-20.5841935944931,24.8106609458197,-61.9812009206874));
#11732=CARTESIAN_POINT('Ctrl Pts',(-20.5825634353728,24.8068178569613,-61.9814566794468));
#11733=CARTESIAN_POINT('Ctrl Pts',(-20.5797617763984,24.8001771032373,-61.9818987023175));
#11734=CARTESIAN_POINT('Ctrl Pts',(-20.5785867477028,24.7973809252438,-61.9820848459707));
#11735=CARTESIAN_POINT('Ctrl Pts',(-20.5761648426371,24.7915947388131,-61.9824700882057));
#11736=CARTESIAN_POINT('Ctrl Pts',(-20.5749185242576,24.7886045016277,-61.9826692055228));
#11737=CARTESIAN_POINT('Ctrl Pts',(-20.571912271326,24.7813609930827,-61.9831516157349));
#11738=CARTESIAN_POINT('Ctrl Pts',(-20.5701569398472,24.7771058290956,-61.9834350646395));
#11739=CARTESIAN_POINT('Ctrl Pts',(-20.5636712424566,24.7612875630612,-61.9844889965752));
#11740=CARTESIAN_POINT('Ctrl Pts',(-20.5589990583004,24.7497008612477,-61.9852614482217));
#11741=CARTESIAN_POINT('Ctrl Pts',(-20.4848186567125,24.5626092366427,-61.997742513382));
#11742=CARTESIAN_POINT('Ctrl Pts',(-20.4308074762157,24.3813906609703,-62.0099815479479));
#11743=CARTESIAN_POINT('Ctrl Pts',(-20.3513804906614,23.9933544786537,-62.0364187489923));
#11744=CARTESIAN_POINT('Ctrl Pts',(-20.3295031678759,23.7866639580283,-62.0506333474106));
#11745=CARTESIAN_POINT('Ctrl Pts',(-20.3267327588802,23.479409023347,-62.0710991096281));
#11746=CARTESIAN_POINT('Ctrl Pts',(-20.3304777694658,23.3795089421442,-62.0776414127557));
#11747=CARTESIAN_POINT('Ctrl Pts',(-20.3400050391837,23.2663244713403,-62.0848122597754));
#11748=CARTESIAN_POINT('Ctrl Pts',(-20.3412371879281,23.2527216157348,-62.085670068894));
#11749=CARTESIAN_POINT('Ctrl Pts',(-20.3429032318838,23.2355447582734,-62.0867478441924));
#11750=CARTESIAN_POINT('Ctrl Pts',(-20.3432566604662,23.2319633614828,-62.0869722640727));
#11751=CARTESIAN_POINT('Ctrl Pts',(-20.343827567743,23.2262756858819,-62.0873281880227));
#11752=CARTESIAN_POINT('Ctrl Pts',(-20.3440411231885,23.2241690299619,-62.0874599137077));
#11753=CARTESIAN_POINT('Ctrl Pts',(-20.3444472656888,23.2202015375728,-62.087707794933));
#11754=CARTESIAN_POINT('Ctrl Pts',(-20.3446393954115,23.2183406717345,-62.0878239753032));
#11755=CARTESIAN_POINT('Ctrl Pts',(-20.3450785134423,23.2141235563539,-62.0880870777551));
#11756=CARTESIAN_POINT('Ctrl Pts',(-20.3453264792661,23.2117674154667,-62.0882339434872));
#11757=CARTESIAN_POINT('Ctrl Pts',(-20.3459713399025,23.2057042683597,-62.0886115438097));
#11758=CARTESIAN_POINT('Ctrl Pts',(-20.3463720707907,23.201997661811,-62.0888420614012));
#11759=CARTESIAN_POINT('Ctrl Pts',(-20.3477047032801,23.1898683205135,-62.0895953668878));
#11760=CARTESIAN_POINT('Ctrl Pts',(-20.3486634036319,23.1814484755917,-62.0901166633395));
#11761=CARTESIAN_POINT('Ctrl Pts',(-20.3693639182988,23.0058109526296,-62.1009587418149));
#11762=CARTESIAN_POINT('Ctrl Pts',(-20.4021507860894,22.8403639021743,-62.1105693997701));
#11763=CARTESIAN_POINT('Ctrl Pts',(-20.5081273151466,22.4633210359709,-62.1325879161485));
#11764=CARTESIAN_POINT('Ctrl Pts',(-20.5906876834503,22.2552936385596,-62.1448622759723));
#11765=CARTESIAN_POINT('Ctrl Pts',(-20.7088431593804,22.0292246008702,-62.1596327993634));
#11766=CARTESIAN_POINT('Ctrl Pts',(-20.7240226705109,22.0012018968284,-62.1614894936866));
#11767=CARTESIAN_POINT('Ctrl Pts',(-20.7792674353832,21.902731084158,-62.1681136090971));
#11768=CARTESIAN_POINT('Ctrl Pts',(-20.8215688465413,21.8335787287641,-62.1729500132687));
#11769=CARTESIAN_POINT('Ctrl Pts',(-20.8717725277658,21.7580595716378,-62.1784722270905));
#11770=CARTESIAN_POINT('Ctrl Pts',(-20.8771524358705,21.7500451514076,-62.1790613782181));
#11771=CARTESIAN_POINT('Ctrl Pts',(-20.8851045870198,21.7383131201855,-62.1799284427673));
#11772=CARTESIAN_POINT('Ctrl Pts',(-20.8876488116961,21.7345765066547,-62.1802052931658));
#11773=CARTESIAN_POINT('Ctrl Pts',(-20.8921176547927,21.728042865872,-62.1806905997266));
#11774=CARTESIAN_POINT('Ctrl Pts',(-20.8940388514819,21.7252434974902,-62.1808989254227));
#11775=CARTESIAN_POINT('Ctrl Pts',(-20.8977702961308,21.7198247974091,-62.1813029451845));
#11776=CARTESIAN_POINT('Ctrl Pts',(-20.8995800100092,21.7172051010254,-62.1814986187122));
#11777=CARTESIAN_POINT('Ctrl Pts',(-20.9038977064244,21.7109746764893,-62.1819648214144));
#11778=CARTESIAN_POINT('Ctrl Pts',(-20.9064091963405,21.7073663963932,-62.1822354846383));
#11779=CARTESIAN_POINT('Ctrl Pts',(-20.9153550660107,21.6945697096346,-62.18319776773));
#11780=CARTESIAN_POINT('Ctrl Pts',(-20.9218299695554,21.6854098518756,-62.1838909420388));
#11781=CARTESIAN_POINT('Ctrl Pts',(-21.016699183305,21.5526767772343,-62.1939999406068));
#11782=CARTESIAN_POINT('Ctrl Pts',(-21.1136623173755,21.4354907574709,-62.2037542518211));
#11783=CARTESIAN_POINT('Ctrl Pts',(-21.3930926163032,21.1426108747191,-62.2304735866183));
#11784=CARTESIAN_POINT('Ctrl Pts',(-21.5885806467701,20.9808358139375,-62.2478871123605));
#11785=CARTESIAN_POINT('Ctrl Pts',(-21.8636517967265,20.8030596873818,-62.2696505202607));
#11786=CARTESIAN_POINT('Ctrl Pts',(-21.9277439989716,20.7647259403196,-62.2745441919646));
#11787=CARTESIAN_POINT('Ctrl Pts',(-22.0197788868993,20.713935289081,-62.2812686352434));
#11788=CARTESIAN_POINT('Ctrl Pts',(-22.0466516300653,20.6995982955594,-62.2831969257403));
#11789=CARTESIAN_POINT('Ctrl Pts',(-22.0777324507544,20.6835780642153,-62.2853836406415));
#11790=CARTESIAN_POINT('Ctrl Pts',(-22.081744501315,20.6815207462935,-62.2856650865714));
#11791=CARTESIAN_POINT('Ctrl Pts',(-22.0878397184095,20.6784113501128,-62.2860914010768));
#11792=CARTESIAN_POINT('Ctrl Pts',(-22.0899197108676,20.6773531145224,-62.2862366576556));
#11793=CARTESIAN_POINT('Ctrl Pts',(-22.0935079289406,20.6755324443012,-62.2864868543271));
#11794=CARTESIAN_POINT('Ctrl Pts',(-22.0950156029074,20.674768937643,-62.2865918625836));
#11795=CARTESIAN_POINT('Ctrl Pts',(-22.0981484773234,20.673185502358,-62.2868098197411));
#11796=CARTESIAN_POINT('Ctrl Pts',(-22.0997737675708,20.6723657669166,-62.2869227562161));
#11797=CARTESIAN_POINT('Ctrl Pts',(-22.1037452255707,20.6703669314353,-62.2871983894458));
#11798=CARTESIAN_POINT('Ctrl Pts',(-22.1060921464365,20.6691893183969,-62.2873609919339));
#11799=CARTESIAN_POINT('Ctrl Pts',(-22.1150308437734,20.6647178204092,-62.2879792313528));
#11800=CARTESIAN_POINT('Ctrl Pts',(-22.1216325381559,20.6614436456489,-62.2884336347802));
#11801=CARTESIAN_POINT('Ctrl Pts',(-22.230842276655,20.6077459370177,-62.2959153895035));
#11802=CARTESIAN_POINT('Ctrl Pts',(-22.3360642199086,20.5627884214963,-62.302611188023));
#11803=CARTESIAN_POINT('Ctrl Pts',(-22.6690472797993,20.4410265493185,-62.3229049184307));
#11804=CARTESIAN_POINT('Ctrl Pts',(-22.9031468271983,20.3840129468366,-62.3359772564061));
#11805=CARTESIAN_POINT('Ctrl Pts',(-23.2343049398447,20.3416603243391,-62.3550312894282));
#11806=CARTESIAN_POINT('Ctrl Pts',(-23.3276598442164,20.3338357040676,-62.360455106484));
#11807=CARTESIAN_POINT('Ctrl Pts',(-23.4622360027322,20.3284431262117,-62.3684309047034));
#11808=CARTESIAN_POINT('Ctrl Pts',(-23.5032803639214,20.3275834294528,-62.3708840939603));
#11809=CARTESIAN_POINT('Ctrl Pts',(-23.5685923387425,20.3274633756572,-62.374825992673));
#11810=CARTESIAN_POINT('Ctrl Pts',(-23.5928552597299,20.3276927959466,-62.3762987621908));
#11811=CARTESIAN_POINT('Ctrl Pts',(-23.6234727235933,20.3283281327724,-62.3781685398715));
#11812=CARTESIAN_POINT('Ctrl Pts',(-23.6298322316303,20.3284789364037,-62.3785575227649));
#11813=CARTESIAN_POINT('Ctrl Pts',(-23.6400005541772,20.3287501839772,-62.3791804701335));
#11814=CARTESIAN_POINT('Ctrl Pts',(-23.6438096963675,20.3288585569333,-62.3794140552171));
#11815=CARTESIAN_POINT('Ctrl Pts',(-23.6509664739983,20.3290748770682,-62.3798533482555));
#11816=CARTESIAN_POINT('Ctrl Pts',(-23.6543141536537,20.329181287599,-62.3800590076558));
#11817=CARTESIAN_POINT('Ctrl Pts',(-23.6618161336828,20.3294314556131,-62.3805202728352));
#11818=CARTESIAN_POINT('Ctrl Pts',(-23.6659703284949,20.3295780320494,-62.3807759668515));
#11819=CARTESIAN_POINT('Ctrl Pts',(-23.676490800429,20.3299696168554,-62.3814241998514));
#11820=CARTESIAN_POINT('Ctrl Pts',(-23.6828566345688,20.3302254661149,-62.3818170788938));
#11821=CARTESIAN_POINT('Ctrl Pts',(-23.7174903061648,20.3317203047429,-62.3839580800118));
#11822=CARTESIAN_POINT('Ctrl Pts',(-23.7457409289805,20.333312623438,-62.3857172724736));
#11823=CARTESIAN_POINT('Ctrl Pts',(-24.091829914779,20.357395181265,-62.4074317872797));
#11824=CARTESIAN_POINT('Ctrl Pts',(-24.4045950293081,20.4265295130346,-62.4290099421752));
#11825=CARTESIAN_POINT('Ctrl Pts',(-24.7786221275252,20.569657068396,-62.4560425755213));
#11826=CARTESIAN_POINT('Ctrl Pts',(-24.8540616491972,20.6018759880461,-62.4615467381371));
#11827=CARTESIAN_POINT('Ctrl Pts',(-24.9988732268713,20.6703690472296,-62.472120824355));
#11828=CARTESIAN_POINT('Ctrl Pts',(-25.068320166187,20.7063636856155,-62.4771955609474));
#11829=CARTESIAN_POINT('Ctrl Pts',(-25.1432570223598,20.74873215936,-62.4826215037508));
#11830=CARTESIAN_POINT('Ctrl Pts',(-25.1501049739293,20.7526371417596,-62.4831168673716));
#11831=CARTESIAN_POINT('Ctrl Pts',(-25.1618891822604,20.7594143989086,-62.4839683946189));
#11832=CARTESIAN_POINT('Ctrl Pts',(-25.1668322215718,20.7622747189556,-62.4843253003983));
#11833=CARTESIAN_POINT('Ctrl Pts',(-25.1740409734131,20.7664717251891,-62.4848453620297));
#11834=CARTESIAN_POINT('Ctrl Pts',(-25.1763126587578,20.7677980495115,-62.4850091848551));
#11835=CARTESIAN_POINT('Ctrl Pts',(-25.1802302218914,20.7700917563712,-62.4852915870889));
#11836=CARTESIAN_POINT('Ctrl Pts',(-25.1818768662564,20.7710578213288,-62.4854102528117));
#11837=CARTESIAN_POINT('Ctrl Pts',(-25.1850400806851,20.7729174185853,-62.4856381425463));
#11838=CARTESIAN_POINT('Ctrl Pts',(-25.1865567743211,20.7738107285148,-62.4857473809007));
#11839=CARTESIAN_POINT('Ctrl Pts',(-25.1901418630547,20.7759262503383,-62.4860055244796));
#11840=CARTESIAN_POINT('Ctrl Pts',(-25.1922096283363,20.777149535517,-62.4861543592084));
#11841=CARTESIAN_POINT('Ctrl Pts',(-25.1983543800792,20.7807940387998,-62.4865964938784));
#11842=CARTESIAN_POINT('Ctrl Pts',(-25.2024274158445,20.7832219573462,-62.4868893579577));
#11843=CARTESIAN_POINT('Ctrl Pts',(-25.2394591385469,20.8054073210776,-62.4895503358395));
#11844=CARTESIAN_POINT('Ctrl Pts',(-25.272069117675,20.8257448412113,-62.491881164575));
#11845=CARTESIAN_POINT('Ctrl Pts',(-25.3141120154441,20.8530217617458,-62.4948804968314));
#11846=CARTESIAN_POINT('Ctrl Pts',(-25.3238802412992,20.8594350239051,-62.495576949496));
#11847=CARTESIAN_POINT('Ctrl Pts',(-25.585061092671,21.0329517169793,-62.5141936240352));
#11848=CARTESIAN_POINT('Ctrl Pts',(-25.8118198727742,21.2345209136155,-62.5303571584884));
#11849=CARTESIAN_POINT('Ctrl Pts',(-26.0705907974369,21.5393821136638,-62.553136679786));
#11850=CARTESIAN_POINT('Ctrl Pts',(-26.1305141550632,21.6168740396499,-62.5587978570835));
#11851=CARTESIAN_POINT('Ctrl Pts',(-26.2233705947597,21.7489756352637,-62.5683528354367));
#11852=CARTESIAN_POINT('Ctrl Pts',(-26.2583781256126,21.8020495837787,-62.5721674979254));
#11853=CARTESIAN_POINT('Ctrl Pts',(-26.2962061472483,21.8632650320275,-62.5765539364127));
#11854=CARTESIAN_POINT('Ctrl Pts',(-26.30059263444,21.8704259335206,-62.5770668462303));
#11855=CARTESIAN_POINT('Ctrl Pts',(-26.3071414192618,21.8812111796943,-62.5778390714714));
#11856=CARTESIAN_POINT('Ctrl Pts',(-26.309324691286,21.8848228000702,-62.5780976164736));
#11857=CARTESIAN_POINT('Ctrl Pts',(-26.3130681012696,21.8910428015224,-62.5785428101684));
#11858=CARTESIAN_POINT('Ctrl Pts',(-26.3146316588432,21.8936491266925,-62.5787293333504));
#11859=CARTESIAN_POINT('Ctrl Pts',(-26.3178447622879,21.8990223283942,-62.5791138235098));
#11860=CARTESIAN_POINT('Ctrl Pts',(-26.3194938510238,21.9017894734719,-62.5793118069436));
#11861=CARTESIAN_POINT('Ctrl Pts',(-26.3234549781928,21.9084589007506,-62.5797889324758));
#11862=CARTESIAN_POINT('Ctrl Pts',(-26.3257629280068,21.912363592997,-62.5800682233375));
#11863=CARTESIAN_POINT('Ctrl Pts',(-26.3328241096206,21.9243677966459,-62.5809267099883));
#11864=CARTESIAN_POINT('Ctrl Pts',(-26.3375501553278,21.9324831685786,-62.5815068928365));
#11865=CARTESIAN_POINT('Ctrl Pts',(-26.3548417410275,21.9624762699824,-62.5836505324463));
#11866=CARTESIAN_POINT('Ctrl Pts',(-26.3671854592183,21.98448022584,-62.5852219731323));
#11867=CARTESIAN_POINT('Ctrl Pts',(-26.3821602589964,22.0119246679084,-62.5871809053969));
#11868=CARTESIAN_POINT('Ctrl Pts',(-26.38503633115,22.0172310700057,-62.5875596176597));
#11869=CARTESIAN_POINT('Ctrl Pts',(-26.3911517994245,22.028590268529,-62.5883702156668));
#11870=CARTESIAN_POINT('Ctrl Pts',(-26.3943867912183,22.0346453909224,-62.5888022542491));
#11871=CARTESIAN_POINT('Ctrl Pts',(-26.3983128664709,22.042050889778,-62.5893305787049));
#11872=CARTESIAN_POINT('Ctrl Pts',(-26.3990223949101,22.0433915130109,-62.5894262191064));
#11873=CARTESIAN_POINT('Ctrl Pts',(-26.4028668559724,22.05066787578,-62.5899453028994));
#11874=CARTESIAN_POINT('Ctrl Pts',(-26.4059841654655,22.0566128635963,-62.5903693589371));
#11875=CARTESIAN_POINT('Ctrl Pts',(-26.4117177282151,22.0676308431104,-62.5911551866483));
#11876=CARTESIAN_POINT('Ctrl Pts',(-26.4143391269476,22.0727011394984,-62.5915167787588));
#11877=CARTESIAN_POINT('Ctrl Pts',(-26.4233210091737,22.0901875665082,-62.5927637294659));
#11878=CARTESIAN_POINT('Ctrl Pts',(-26.4296142669598,22.1026378845407,-62.593651371961));
#11879=CARTESIAN_POINT('Ctrl Pts',(-26.4418201580501,22.1271800148201,-62.5954007725723));
#11880=CARTESIAN_POINT('Ctrl Pts',(-26.4477382730089,22.139268798126,-62.5962623260977));
#11881=CARTESIAN_POINT('Ctrl Pts',(-26.5189800641106,22.2871309996907,-62.6067985072832));
#11882=CARTESIAN_POINT('Ctrl Pts',(-26.5747724853271,22.4272706406842,-62.6167795648067));
#11883=CARTESIAN_POINT('Ctrl Pts',(-26.702982982022,22.8291665877747,-62.6451666043849));
#11884=CARTESIAN_POINT('Ctrl Pts',(-26.7524699199394,23.0969343249204,-62.6638799285124));
#11885=CARTESIAN_POINT('Ctrl Pts',(-26.768514041884,23.3797943424662,-62.6817396378307));
#11886=CARTESIAN_POINT('Ctrl Pts',(-26.7691296772904,23.3918445937908,-62.6824967211706));
#11887=CARTESIAN_POINT('Ctrl Pts',(-26.7698326388904,23.4073079755048,-62.6834631657312));
#11888=CARTESIAN_POINT('Ctrl Pts',(-26.7699822283031,23.4107179702774,-62.6836759701472));
#11889=CARTESIAN_POINT('Ctrl Pts',(-26.7702140841203,23.4162022695238,-62.6840177077187));
#11890=CARTESIAN_POINT('Ctrl Pts',(-26.7702997637458,23.4182764152723,-62.6841468331699));
#11891=CARTESIAN_POINT('Ctrl Pts',(-26.7704591843564,23.4222282843805,-62.6843926278519));
#11892=CARTESIAN_POINT('Ctrl Pts',(-26.7705332865564,23.4241059755363,-62.6845093164454));
#11893=CARTESIAN_POINT('Ctrl Pts',(-26.7706983377364,23.4283831806955,-62.6847748997444));
#11894=CARTESIAN_POINT('Ctrl Pts',(-26.7707882471821,23.4307827291293,-62.684923734947));
#11895=CARTESIAN_POINT('Ctrl Pts',(-26.7710594895735,23.4382446611005,-62.6853860821668));
#11896=CARTESIAN_POINT('Ctrl Pts',(-26.7712315697593,23.4433074047653,-62.6856990738291));
#11897=CARTESIAN_POINT('Ctrl Pts',(-26.7724552319534,23.4819951796002,-62.6880856453007));
#11898=CARTESIAN_POINT('Ctrl Pts',(-26.7729922391513,23.5156360039366,-62.6901308417443));
#11899=CARTESIAN_POINT('Ctrl Pts',(-26.7730296419443,23.6396655684802,-62.6975807248413));
#11900=CARTESIAN_POINT('Ctrl Pts',(-26.7692544859915,23.7300197869808,-62.7028311695884));
#11901=CARTESIAN_POINT('Ctrl Pts',(-26.7363864459781,24.1211752484018,-62.7252426017645));
#11902=CARTESIAN_POINT('Ctrl Pts',(-26.6688805455199,24.4171860465191,-62.7415343484805));
#11903=CARTESIAN_POINT('Ctrl Pts',(-26.5537003617462,24.7189497494565,-62.7604473963805));
#11904=CARTESIAN_POINT('Ctrl Pts',(-26.5460786432166,24.7383509859413,-62.7616732994514));
#11905=CARTESIAN_POINT('Ctrl Pts',(-26.5361900199105,24.7628223984125,-62.7632328820045));
#11906=CARTESIAN_POINT('Ctrl Pts',(-26.5340973894631,24.7679627720399,-62.7635612299817));
#11907=CARTESIAN_POINT('Ctrl Pts',(-26.5304557374567,24.7768424373042,-62.7641297412657));
#11908=CARTESIAN_POINT('Ctrl Pts',(-26.528912926646,24.7805842737531,-62.7643697121258));
#11909=CARTESIAN_POINT('Ctrl Pts',(-26.5259493637181,24.7877336654344,-62.7648289952333));
#11910=CARTESIAN_POINT('Ctrl Pts',(-26.5245297963266,24.7911417070074,-62.7650482702017));
#11911=CARTESIAN_POINT('Ctrl Pts',(-26.5026524000153,24.8434108799967,-62.7684165475364));
#11912=CARTESIAN_POINT('Ctrl Pts',(-26.4809997975422,24.8917604362934,-62.7716029759637));
#11913=CARTESIAN_POINT('Ctrl Pts',(-26.4544013119957,24.9474331597046,-62.775363038213));
#11914=CARTESIAN_POINT('Ctrl Pts',(-26.4506041641618,24.955298527771,-62.775896398483));
#11915=CARTESIAN_POINT('Ctrl Pts',(-26.444895042529,24.9670025756601,-62.7766933016317));
#11916=CARTESIAN_POINT('Ctrl Pts',(-26.4430072814539,24.9708530772631,-62.7769559983644));
#11917=CARTESIAN_POINT('Ctrl Pts',(-26.4396255958531,24.9777160743321,-62.7774251609249));
#11918=CARTESIAN_POINT('Ctrl Pts',(-26.4381346285709,24.980730026746,-62.777631522954));
#11919=CARTESIAN_POINT('Ctrl Pts',(-26.4349802734148,24.9870814443392,-62.7780670854253));
#11920=CARTESIAN_POINT('Ctrl Pts',(-26.4333158054882,24.9904183649158,-62.7782963235422));
#11921=CARTESIAN_POINT('Ctrl Pts',(-26.4289017080804,24.9992294150238,-62.7789026866957));
#11922=CARTESIAN_POINT('Ctrl Pts',(-26.4261422653967,25.0046985870319,-62.7792801563821));
#11923=CARTESIAN_POINT('Ctrl Pts',(-26.4135642632315,25.0294522432237,-62.7809935726485));
#11924=CARTESIAN_POINT('Ctrl Pts',(-26.4035673955934,25.0486450400871,-62.7823357981142));
#11925=CARTESIAN_POINT('Ctrl Pts',(-26.3287178626129,25.188881639354,-62.7922462555966));
#11926=CARTESIAN_POINT('Ctrl Pts',(-26.2563896371225,25.3057547256251,-62.8010835337991));
#11927=CARTESIAN_POINT('Ctrl Pts',(-26.0142863146747,25.6462853194517,-62.8286491044187));
#11928=CARTESIAN_POINT('Ctrl Pts',(-25.8225997747101,25.8526928507429,-62.848067056912));
#11929=CARTESIAN_POINT('Ctrl Pts',(-25.5964981336581,26.0400657048609,-62.8673736752427));
#11930=CARTESIAN_POINT('Ctrl Pts',(-25.5863152584952,26.0483997016849,-62.8682361720479));
#11931=CARTESIAN_POINT('Ctrl Pts',(-25.5730428972445,26.0591271727087,-62.8693510113248));
#11932=CARTESIAN_POINT('Ctrl Pts',(-25.5699998283481,26.0615776172243,-62.869605988426));
#11933=CARTESIAN_POINT('Ctrl Pts',(-25.5591255267451,26.0703016458713,-62.8705148679604));
#11934=CARTESIAN_POINT('Ctrl Pts',(-25.5512693806771,26.0765442454336,-62.8711672944525));
#11935=CARTESIAN_POINT('Ctrl Pts',(-25.503895134036,26.1138288247311,-62.8750758424063));
#11936=CARTESIAN_POINT('Ctrl Pts',(-25.4636818136582,26.1439818767783,-62.8782866710628));
#11937=CARTESIAN_POINT('Ctrl Pts',(-25.4186205381457,26.1761513561175,-62.8817540334784));
#11938=CARTESIAN_POINT('Ctrl Pts',(-25.4144569966578,26.1791088148145,-62.8820732048896));
#11939=CARTESIAN_POINT('Ctrl Pts',(-25.4082495643326,26.1834959329452,-62.8825472480335));
#11940=CARTESIAN_POINT('Ctrl Pts',(-25.4062110409021,26.1849331187345,-62.8827026344115));
#11941=CARTESIAN_POINT('Ctrl Pts',(-25.4027113003732,26.1873944043916,-62.8829689027244));
#11942=CARTESIAN_POINT('Ctrl Pts',(-25.4012509016124,26.1884196569889,-62.8830798643828));
#11943=CARTESIAN_POINT('Ctrl Pts',(-25.3983944021739,26.1904214830782,-62.8832966102955));
#11944=CARTESIAN_POINT('Ctrl Pts',(-25.396998382076,26.1913981598979,-62.8834024014528));
#11945=CARTESIAN_POINT('Ctrl Pts',(-25.3936113619773,26.1937637721693,-62.8836587427707));
#11946=CARTESIAN_POINT('Ctrl Pts',(-25.3916195611401,26.1951515692122,-62.8838092139799));
#11947=CARTESIAN_POINT('Ctrl Pts',(-25.3854650708664,26.1994294187365,-62.8842733144337));
#11948=CARTESIAN_POINT('Ctrl Pts',(-25.3812971056927,26.2023119223632,-62.884586426134));
#11949=CARTESIAN_POINT('Ctrl Pts',(-25.3340669038983,26.2348112204905,-62.8881213126561));
#11950=CARTESIAN_POINT('Ctrl Pts',(-25.2902940809684,26.2633882176537,-62.8912734879278));
#11951=CARTESIAN_POINT('Ctrl Pts',(-25.196313939655,26.3215322798282,-62.8978267114756));
#11952=CARTESIAN_POINT('Ctrl Pts',(-25.1459610853148,26.3508282862131,-62.9012138446932));
#11953=CARTESIAN_POINT('Ctrl Pts',(-24.7541040524248,26.5648140701814,-62.9268505478225));
#11954=CARTESIAN_POINT('Ctrl Pts',(-24.3825738590906,26.6877861475458,-62.9474804942564));
#11955=CARTESIAN_POINT('Ctrl Pts',(-23.9787156275817,26.7444533208138,-62.9721553109128));
#11956=CARTESIAN_POINT('Ctrl Pts',(-23.9593429708257,26.7469921664156,-62.9733429127609));
#11957=CARTESIAN_POINT('Ctrl Pts',(-23.9338444105501,26.7500982543653,-62.9749116467279));
#11958=CARTESIAN_POINT('Ctrl Pts',(-23.9277379868606,26.7508243725893,-62.9752877497374));
#11959=CARTESIAN_POINT('Ctrl Pts',(-23.9182910665249,26.7519202994187,-62.9758702614111));
#11960=CARTESIAN_POINT('Ctrl Pts',(-23.9149519837663,26.7523023700833,-62.9760762823862));
#11961=CARTESIAN_POINT('Ctrl Pts',(-23.9082887793482,26.753054241827,-62.9764876590106));
#11962=CARTESIAN_POINT('Ctrl Pts',(-23.9049646673983,26.7534240927746,-62.9766930128162));
#11963=CARTESIAN_POINT('Ctrl Pts',(-23.8976579043937,26.7542255523907,-62.9771446867289));
#11964=CARTESIAN_POINT('Ctrl Pts',(-23.8936750166733,26.754654910752,-62.9773910775577));
#11965=CARTESIAN_POINT('Ctrl Pts',(-23.8822530248263,26.7558646705007,-62.9780982052926));
#11966=CARTESIAN_POINT('Ctrl Pts',(-23.8748120271274,26.7566265966336,-62.9785595245487));
#11967=CARTESIAN_POINT('Ctrl Pts',(-23.8580818229134,26.7582808631508,-62.9795982385057));
#11968=CARTESIAN_POINT('Ctrl Pts',(-23.8487912866435,26.7591587716467,-62.9801760851831));
#11969=CARTESIAN_POINT('Ctrl Pts',(-23.7728664832735,26.7660007011019,-62.9849070135689));
#11970=CARTESIAN_POINT('Ctrl Pts',(-23.7060694212423,26.769928489853,-62.9891238419397));
#11971=CARTESIAN_POINT('Ctrl Pts',(-23.5170219692526,26.7751482996902,-63.0012239128181));
#11972=CARTESIAN_POINT('Ctrl Pts',(-23.3947615790465,26.7715680858433,-63.0092488539537));
#11973=CARTESIAN_POINT('Ctrl Pts',(-23.0554202310777,26.7422671312002,-63.0319944215086));
#11974=CARTESIAN_POINT('Ctrl Pts',(-22.8403137068418,26.7014108521678,-63.0469896945684));
#11975=CARTESIAN_POINT('Ctrl Pts',(-22.5978067973046,26.6292399916863,-63.0637641899935));
#11976=CARTESIAN_POINT('Ctrl Pts',(-22.5647776581904,26.6188281116729,-63.0660447134939));
#11977=CARTESIAN_POINT('Ctrl Pts',(-22.5269223294283,26.6062205658002,-63.0686490018587));
#11978=CARTESIAN_POINT('Ctrl Pts',(-22.521927032972,26.6045432836831,-63.0689924657047));
#11979=CARTESIAN_POINT('Ctrl Pts',(-22.5143130469968,26.6019659215525,-63.0695156687644));
#11980=CARTESIAN_POINT('Ctrl Pts',(-22.511691387665,26.6010747126819,-63.0696957617399));
#11981=CARTESIAN_POINT('Ctrl Pts',(-22.457650155535,26.5826261633041,-63.0734068620372));
#11982=CARTESIAN_POINT('Ctrl Pts',(-22.4066776556992,26.5637732594062,-63.076884487792));
#11983=CARTESIAN_POINT('Ctrl Pts',(-22.3513599449896,26.5417072466894,-63.0806148034183));
#11984=CARTESIAN_POINT('Ctrl Pts',(-22.3465218563873,26.5397637306284,-63.0809406848808));
#11985=CARTESIAN_POINT('Ctrl Pts',(-22.339351921695,26.5368632575939,-63.0814230581751));
#11986=CARTESIAN_POINT('Ctrl Pts',(-22.3370164778092,26.5359153045163,-63.0815800896108));
#11987=CARTESIAN_POINT('Ctrl Pts',(-22.3330230320878,26.5342889116653,-63.0818484440659));
#11988=CARTESIAN_POINT('Ctrl Pts',(-22.331364484321,26.5336118294842,-63.0819598495881));
#11989=CARTESIAN_POINT('Ctrl Pts',(-22.3281327203656,26.532289355876,-63.0821768364364));
#11990=CARTESIAN_POINT('Ctrl Pts',(-22.3265594547524,26.5316441040096,-63.0822824256055));
#11991=CARTESIAN_POINT('Ctrl Pts',(-22.3227605862293,26.5300825401395,-63.0825372829412));
#11992=CARTESIAN_POINT('Ctrl Pts',(-22.3205354929258,26.5291649775485,-63.082686474476));
#11993=CARTESIAN_POINT('Ctrl Pts',(-22.3137258320642,26.5263479451074,-63.0831428055026));
#11994=CARTESIAN_POINT('Ctrl Pts',(-22.3091445945163,26.5244403666656,-63.0834494522744));
#11995=CARTESIAN_POINT('Ctrl Pts',(-22.2615659988413,26.5045000720646,-63.0866306577157));
#11996=CARTESIAN_POINT('Ctrl Pts',(-22.2189576330256,26.4855456964201,-63.0894499294728));
#11997=CARTESIAN_POINT('Ctrl Pts',(-22.1425667982278,26.4495573079125,-63.0944767463532));
#11998=CARTESIAN_POINT('Ctrl Pts',(-22.108649264616,26.4328428484025,-63.0966984848586));
#11999=CARTESIAN_POINT('Ctrl Pts',(-22.0750360104957,26.415536772059,-63.0988976931332));
#12000=CARTESIAN_POINT('Ctrl Pts',(-22.0750360636209,26.415536799411,-63.3454515897691));
#12001=CARTESIAN_POINT('Ctrl Pts',(-22.1035139487319,26.4301988856706,-63.3433761302491));
#12002=CARTESIAN_POINT('Ctrl Pts',(-22.1322130926595,26.4444377881483,-63.3412872344756));
#12003=CARTESIAN_POINT('Ctrl Pts',(-22.3859690724233,26.5656551589085,-63.3228442277982));
#12004=CARTESIAN_POINT('Ctrl Pts',(-22.6225025957412,26.6466157135218,-63.3057439062922));
#12005=CARTESIAN_POINT('Ctrl Pts',(-22.978130535227,26.7238894805538,-63.2813865433741));
#12006=CARTESIAN_POINT('Ctrl Pts',(-23.0915422963139,26.7422559987677,-63.2738263129914));
#12007=CARTESIAN_POINT('Ctrl Pts',(-23.2202814139249,26.7560989991967,-63.2656450607918));
#12008=CARTESIAN_POINT('Ctrl Pts',(-23.2348693926878,26.7575669857108,-63.264723802468));
#12009=CARTESIAN_POINT('Ctrl Pts',(-23.2531043774595,26.7592763524494,-63.2635798902177));
#12010=CARTESIAN_POINT('Ctrl Pts',(-23.256742144084,26.7596111218832,-63.2633520673186));
#12011=CARTESIAN_POINT('Ctrl Pts',(-23.2625015076198,26.7601312593157,-63.2629919856033));
#12012=CARTESIAN_POINT('Ctrl Pts',(-23.2646227184901,26.7603207097498,-63.2628594962701));
#12013=CARTESIAN_POINT('Ctrl Pts',(-23.2686059991718,26.760672486597,-63.2626109514942));
#12014=CARTESIAN_POINT('Ctrl Pts',(-23.270468009301,26.760835294554,-63.262494869667));
#12015=CARTESIAN_POINT('Ctrl Pts',(-23.2746721811723,26.7611992081428,-63.2622330016139));
#12016=CARTESIAN_POINT('Ctrl Pts',(-23.2770144173696,26.761399370686,-63.2620872696178));
#12017=CARTESIAN_POINT('Ctrl Pts',(-23.2830123156982,26.7619053284252,-63.2617144913091));
#12018=CARTESIAN_POINT('Ctrl Pts',(-23.2866682960382,26.762207445888,-63.2614876527409));
#12019=CARTESIAN_POINT('Ctrl Pts',(-23.3059908557881,26.7637709816636,-63.2602907694939));
#12020=CARTESIAN_POINT('Ctrl Pts',(-23.3216663453432,26.7649240504745,-63.2593267481727));
#12021=CARTESIAN_POINT('Ctrl Pts',(-23.6600138783291,26.7873250267285,-63.2386567153596));
#12022=CARTESIAN_POINT('Ctrl Pts',(-23.9841160071203,26.7600082673915,-63.2214197319263));
#12023=CARTESIAN_POINT('Ctrl Pts',(-24.4512899805282,26.6484517226613,-63.1941780772581));
#12024=CARTESIAN_POINT('Ctrl Pts',(-24.6009298841737,26.6009531100718,-63.1850888061931));
#12025=CARTESIAN_POINT('Ctrl Pts',(-24.7607399143834,26.5370690309539,-63.1746955149162));
#12026=CARTESIAN_POINT('Ctrl Pts',(-24.7749316783804,26.5312781067341,-63.173766549716));
#12027=CARTESIAN_POINT('Ctrl Pts',(-24.7961802523034,26.5224303205561,-63.1723664074307));
#12028=CARTESIAN_POINT('Ctrl Pts',(-24.8032684480307,26.5194490232362,-63.1718977865457));
#12029=CARTESIAN_POINT('Ctrl Pts',(-24.8146645151413,26.5146077592847,-63.1711418256016));
#12030=CARTESIAN_POINT('Ctrl Pts',(-24.8189791421654,26.5127636906172,-63.1708550268203));
#12031=CARTESIAN_POINT('Ctrl Pts',(-24.8272189873183,26.5092206841843,-63.1703061839863));
#12032=CARTESIAN_POINT('Ctrl Pts',(-24.8311448835312,26.5075233408975,-63.1700441947972));
#12033=CARTESIAN_POINT('Ctrl Pts',(-24.8381037037438,26.5044982700589,-63.1695789302769));
#12034=CARTESIAN_POINT('Ctrl Pts',(-24.8411379883901,26.5031736721166,-63.1693757623662));
#12035=CARTESIAN_POINT('Ctrl Pts',(-24.8471181423081,26.5005520945917,-63.168974758992));
#12036=CARTESIAN_POINT('Ctrl Pts',(-24.8500641210113,26.4992553724823,-63.1687769325387));
#12037=CARTESIAN_POINT('Ctrl Pts',(-24.8571478756867,26.496124661828,-63.1683005678536));
#12038=CARTESIAN_POINT('Ctrl Pts',(-24.861283732456,26.4942863693993,-63.168021881915));
#12039=CARTESIAN_POINT('Ctrl Pts',(-24.873952466886,26.4886234208464,-63.1671664992016));
#12040=CARTESIAN_POINT('Ctrl Pts',(-24.8824725253425,26.4847703602664,-63.1665888251262));
#12041=CARTESIAN_POINT('Ctrl Pts',(-24.9808813222323,26.4397496491777,-63.1598883800592));
#12042=CARTESIAN_POINT('Ctrl Pts',(-25.0688376918065,26.3945077905284,-63.1536244795885));
#12043=CARTESIAN_POINT('Ctrl Pts',(-25.1863239032119,26.3270724095538,-63.1448589268642));
#12044=CARTESIAN_POINT('Ctrl Pts',(-25.2177650500524,26.3083061951901,-63.1424724823351));
#12045=CARTESIAN_POINT('Ctrl Pts',(-25.3222928713269,26.2434761510015,-63.1344026282554));
#12046=CARTESIAN_POINT('Ctrl Pts',(-25.393842241216,26.195012596739,-63.1286498909912));
#12047=CARTESIAN_POINT('Ctrl Pts',(-25.5163415004817,26.1046501216796,-63.1184220055215));
#12048=CARTESIAN_POINT('Ctrl Pts',(-25.5681170393693,26.0639500881644,-63.1139709549432));
#12049=CARTESIAN_POINT('Ctrl Pts',(-25.7273133536302,25.9307182357265,-63.0999203799137));
#12050=CARTESIAN_POINT('Ctrl Pts',(-25.8299029366639,25.8326654897099,-63.0903097588793));
#12051=CARTESIAN_POINT('Ctrl Pts',(-25.9746713442664,25.6747667368957,-63.0762088016034));
#12052=CARTESIAN_POINT('Ctrl Pts',(-26.0218252535001,25.6197204224106,-63.0715177587804));
#12053=CARTESIAN_POINT('Ctrl Pts',(-26.0741989217383,25.5542340277822,-63.0662350712626));
#12054=CARTESIAN_POINT('Ctrl Pts',(-26.0812637262964,25.5453037988384,-63.0655208768525));
#12055=CARTESIAN_POINT('Ctrl Pts',(-26.0903410872506,25.5337037826833,-63.0646013529052));
#12056=CARTESIAN_POINT('Ctrl Pts',(-26.0923969125697,25.5310681925127,-63.0643929748548));
#12057=CARTESIAN_POINT('Ctrl Pts',(-26.0957131903058,25.5268030223526,-63.064056640423));
#12058=CARTESIAN_POINT('Ctrl Pts',(-26.0969761802651,25.5251754326016,-63.063928502486));
#12059=CARTESIAN_POINT('Ctrl Pts',(-26.0993909705785,25.5220573724472,-63.0636834203105));
#12060=CARTESIAN_POINT('Ctrl Pts',(-26.1005430212296,25.5205671080027,-63.0635664583828));
#12061=CARTESIAN_POINT('Ctrl Pts',(-26.1031796952898,25.5171501843355,-63.0632986815936));
#12062=CARTESIAN_POINT('Ctrl Pts',(-26.1046634478468,25.5152228495679,-63.0631479292423));
#12063=CARTESIAN_POINT('Ctrl Pts',(-26.1085948985283,25.5101040753022,-63.0627483084962));
#12064=CARTESIAN_POINT('Ctrl Pts',(-26.1110388165535,25.5069097174612,-63.0624997083793));
#12065=CARTESIAN_POINT('Ctrl Pts',(-26.122589290469,25.4917537985796,-63.0613238588694));
#12066=CARTESIAN_POINT('Ctrl Pts',(-26.1316182480043,25.4797329356285,-63.0604020040766));
#12067=CARTESIAN_POINT('Ctrl Pts',(-26.3203626568914,25.2247483227428,-63.0410634350453));
#12068=CARTESIAN_POINT('Ctrl Pts',(-26.4651372110138,24.9577196598887,-63.0248169297578));
#12069=CARTESIAN_POINT('Ctrl Pts',(-26.6386900582848,24.4914150159533,-62.9967477022875));
#12070=CARTESIAN_POINT('Ctrl Pts',(-26.6900121573599,24.3026652985737,-62.9854767671159));
#12071=CARTESIAN_POINT('Ctrl Pts',(-26.7256675859307,24.1006664605714,-62.9729875210343));
#12072=CARTESIAN_POINT('Ctrl Pts',(-26.7273492221113,24.0908752060603,-62.9723812038139));
#12073=CARTESIAN_POINT('Ctrl Pts',(-26.7297301665049,24.0766173952489,-62.9714968798542));
#12074=CARTESIAN_POINT('Ctrl Pts',(-26.7304654025858,24.0721568287941,-62.971220016844));
#12075=CARTESIAN_POINT('Ctrl Pts',(-26.7317364112952,24.0643433943958,-62.9707346862915));
#12076=CARTESIAN_POINT('Ctrl Pts',(-26.7322762764907,24.0609911915612,-62.9705263492244));
#12077=CARTESIAN_POINT('Ctrl Pts',(-26.7333121587167,24.0544936570366,-62.970122306027));
#12078=CARTESIAN_POINT('Ctrl Pts',(-26.7338088139923,24.0513484296874,-62.9699266204353));
#12079=CARTESIAN_POINT('Ctrl Pts',(-26.7349801277713,24.043858681727,-62.969460386801));
#12080=CARTESIAN_POINT('Ctrl Pts',(-26.7356505575562,24.0395135143022,-62.969189704688));
#12081=CARTESIAN_POINT('Ctrl Pts',(-26.7380000627026,24.0240764346929,-62.9682273427169));
#12082=CARTESIAN_POINT('Ctrl Pts',(-26.7396300965444,24.0129772405787,-62.9675341081391));
#12083=CARTESIAN_POINT('Ctrl Pts',(-26.762498491901,23.8513981996924,-62.9574227261462));
#12084=CARTESIAN_POINT('Ctrl Pts',(-26.7731218037237,23.6996320371111,-62.9476659204347));
#12085=CARTESIAN_POINT('Ctrl Pts',(-26.7728665898019,23.3772651636872,-62.9263872116026));
#12086=CARTESIAN_POINT('Ctrl Pts',(-26.759211452541,23.2071191544008,-62.9148246348769));
#12087=CARTESIAN_POINT('Ctrl Pts',(-26.7039187291296,22.8630800974918,-62.8912611082392));
#12088=CARTESIAN_POINT('Ctrl Pts',(-26.6611445797017,22.689913216979,-62.879306223084));
#12089=CARTESIAN_POINT('Ctrl Pts',(-26.6006844667297,22.5104885636931,-62.8673772125349));
#12090=CARTESIAN_POINT('Ctrl Pts',(-26.5970365743858,22.4998473215232,-62.8666715567893));
#12091=CARTESIAN_POINT('Ctrl Pts',(-26.5921909229873,22.4859497462818,-62.8657525578943));
#12092=CARTESIAN_POINT('Ctrl Pts',(-26.5910435761106,22.4826761082344,-62.865536272407));
#12093=CARTESIAN_POINT('Ctrl Pts',(-26.5892662855374,22.4776312096369,-62.8652032603495));
#12094=CARTESIAN_POINT('Ctrl Pts',(-26.5886400783641,22.4758586500735,-62.8650863111906));
#12095=CARTESIAN_POINT('Ctrl Pts',(-26.5874516223016,22.4725039219197,-62.8648650835445));
#12096=CARTESIAN_POINT('Ctrl Pts',(-26.5868896907671,22.470921652852,-62.8647607869308));
#12097=CARTESIAN_POINT('Ctrl Pts',(-26.5855809357767,22.46724561416,-62.8645185846458));
#12098=CARTESIAN_POINT('Ctrl Pts',(-26.5848331836357,22.4651521810395,-62.8643807355553));
#12099=CARTESIAN_POINT('Ctrl Pts',(-26.5827078419135,22.4592213785626,-62.8639904256466));
#12100=CARTESIAN_POINT('Ctrl Pts',(-26.581325129184,22.4553858298703,-62.8637382711967));
#12101=CARTESIAN_POINT('Ctrl Pts',(-26.5728640511415,22.4320542659334,-62.8622059784853));
#12102=CARTESIAN_POINT('Ctrl Pts',(-26.565604678674,22.4126237511553,-62.8609365124723));
#12103=CARTESIAN_POINT('Ctrl Pts',(-26.5432795348477,22.3545834813715,-62.8571606157347));
#12104=CARTESIAN_POINT('Ctrl Pts',(-26.527655552367,22.3161914603863,-62.8546844516276));
#12105=CARTESIAN_POINT('Ctrl Pts',(-26.4803758370018,22.2061431182659,-62.8476197956409));
#12106=CARTESIAN_POINT('Ctrl Pts',(-26.4468416806164,22.135323001619,-62.8431143964127));
#12107=CARTESIAN_POINT('Ctrl Pts',(-26.2456394413674,21.7476132820124,-62.818311408195));
#12108=CARTESIAN_POINT('Ctrl Pts',(-26.0286163946755,21.4592391607728,-62.7990023840234));
#12109=CARTESIAN_POINT('Ctrl Pts',(-25.753720002155,21.198387695362,-62.7760860337717));
#12110=CARTESIAN_POINT('Ctrl Pts',(-25.7387281911664,21.1844310338759,-62.7748414463933));
#12111=CARTESIAN_POINT('Ctrl Pts',(-25.7189785277042,21.166393398115,-62.7732081498128));
#12112=CARTESIAN_POINT('Ctrl Pts',(-25.7143401479284,21.162181845365,-62.772825002185));
#12113=CARTESIAN_POINT('Ctrl Pts',(-25.7071773423082,21.1557161720927,-62.7722339999794));
#12114=CARTESIAN_POINT('Ctrl Pts',(-25.7046615791716,21.1534524415522,-62.7720265517588));
#12115=CARTESIAN_POINT('Ctrl Pts',(-25.69965371839,21.1489605301881,-62.7716138564955));
#12116=CARTESIAN_POINT('Ctrl Pts',(-25.6971617101518,21.1467322556852,-62.7714086137748));
#12117=CARTESIAN_POINT('Ctrl Pts',(-25.6916428910609,21.1418129342232,-62.7709543495192));
#12118=CARTESIAN_POINT('Ctrl Pts',(-25.6886144688717,21.1391237107379,-62.7707052519067));
#12119=CARTESIAN_POINT('Ctrl Pts',(-25.6799009155616,21.1314154484729,-62.7699890367332));
#12120=CARTESIAN_POINT('Ctrl Pts',(-25.6742031556735,21.1264107836837,-62.7695213192328));
#12121=CARTESIAN_POINT('Ctrl Pts',(-25.6366426904858,21.0936534368531,-62.7664419905889));
#12122=CARTESIAN_POINT('Ctrl Pts',(-25.6042557294637,21.0665106777939,-62.7638052448538));
#12123=CARTESIAN_POINT('Ctrl Pts',(-25.5070811281415,20.988271546001,-62.7559428242576));
#12124=CARTESIAN_POINT('Ctrl Pts',(-25.440858426241,20.9390206144685,-62.7506460023929));
#12125=CARTESIAN_POINT('Ctrl Pts',(-25.1274617479128,20.7241174857947,-62.7258510622817));
#12126=CARTESIAN_POINT('Ctrl Pts',(-24.8600335440666,20.5906817066048,-62.7052668859013));
#12127=CARTESIAN_POINT('Ctrl Pts',(-24.4921523738601,20.4668823243921,-62.6795854942009));
#12128=CARTESIAN_POINT('Ctrl Pts',(-24.4049799495618,20.4415885434462,-62.673693876368));
#12129=CARTESIAN_POINT('Ctrl Pts',(-24.3106069928732,20.4184766880527,-62.6676027216059));
#12130=CARTESIAN_POINT('Ctrl Pts',(-24.3043619161782,20.4169670548556,-62.6672009766631));
#12131=CARTESIAN_POINT('Ctrl Pts',(-24.2957002693518,20.4149006563931,-62.6666456615151));
#12132=CARTESIAN_POINT('Ctrl Pts',(-24.2932875623938,20.4143280021834,-62.6664911808533));
#12133=CARTESIAN_POINT('Ctrl Pts',(-24.2891413037268,20.4133489444949,-62.6662260554862));
#12134=CARTESIAN_POINT('Ctrl Pts',(-24.2874080766188,20.4129411930729,-62.6661153325817));
#12135=CARTESIAN_POINT('Ctrl Pts',(-24.2838657343958,20.4121109347121,-62.6658892552871));
#12136=CARTESIAN_POINT('Ctrl Pts',(-24.2820565955017,20.4116885565464,-62.6657739089666));
#12137=CARTESIAN_POINT('Ctrl Pts',(-24.2778348910523,20.4107067673773,-62.6655050108711));
#12138=CARTESIAN_POINT('Ctrl Pts',(-24.2754220380741,20.4101485711533,-62.6653515298092));
#12139=CARTESIAN_POINT('Ctrl Pts',(-24.2703278076814,20.4089762423035,-62.6650279120954));
#12140=CARTESIAN_POINT('Ctrl Pts',(-24.2676462804431,20.4083627597949,-62.6648578129903));
#12141=CARTESIAN_POINT('Ctrl Pts',(-24.2604558988529,20.4067274222674,-62.6644023585206));
#12142=CARTESIAN_POINT('Ctrl Pts',(-24.2559456047233,20.4057118301575,-62.6641173595603));
#12143=CARTESIAN_POINT('Ctrl Pts',(-24.1492673494408,20.3819319501476,-62.6573925518916));
#12144=CARTESIAN_POINT('Ctrl Pts',(-24.0460400965875,20.3641461322928,-62.6512323276985));
#12145=CARTESIAN_POINT('Ctrl Pts',(-23.5531680738928,20.3037679866669,-62.6226773451752));
#12146=CARTESIAN_POINT('Ctrl Pts',(-23.1588064848565,20.3274461106527,-62.6018891165103));
#12147=CARTESIAN_POINT('Ctrl Pts',(-22.7595624291082,20.4259447048717,-62.5770051247287));
#12148=CARTESIAN_POINT('Ctrl Pts',(-22.740861936758,20.4307370124734,-62.5758316187693));
#12149=CARTESIAN_POINT('Ctrl Pts',(-22.7162909932846,20.4372695290888,-62.5742788770824));
#12150=CARTESIAN_POINT('Ctrl Pts',(-22.7103805715818,20.438858935272,-62.5739045428731));
#12151=CARTESIAN_POINT('Ctrl Pts',(-22.7012372042796,20.4413456830883,-62.5733241537432));
#12152=CARTESIAN_POINT('Ctrl Pts',(-22.6980010499557,20.4422312590462,-62.573118481869));
#12153=CARTESIAN_POINT('Ctrl Pts',(-22.6915408931245,20.4440099339358,-62.5727074043582));
#12154=CARTESIAN_POINT('Ctrl Pts',(-22.6883168865168,20.4449030026101,-62.572501999925));
#12155=CARTESIAN_POINT('Ctrl Pts',(-22.6811460946831,20.4469013813235,-62.5720445784659));
#12156=CARTESIAN_POINT('Ctrl Pts',(-22.6772000206982,20.4480092023989,-62.5717924798311));
#12157=CARTESIAN_POINT('Ctrl Pts',(-22.6657389075246,20.4512503957857,-62.5710591637199));
#12158=CARTESIAN_POINT('Ctrl Pts',(-22.6582295379145,20.4534035578899,-62.5705773007595));
#12159=CARTESIAN_POINT('Ctrl Pts',(-22.6054329425058,20.4687498948358,-62.5671795399704));
#12160=CARTESIAN_POINT('Ctrl Pts',(-22.5604343489799,20.4829080546418,-62.5642321746569));
#12161=CARTESIAN_POINT('Ctrl Pts',(-22.4203578632667,20.5303843775104,-62.5548884429675));
#12162=CARTESIAN_POINT('Ctrl Pts',(-22.3265289877297,20.567173108523,-62.5483800466649));
#12163=CARTESIAN_POINT('Ctrl Pts',(-22.0833076741205,20.6759436238406,-62.5308488114397));
#12164=CARTESIAN_POINT('Ctrl Pts',(-21.937485711875,20.7551579582102,-62.5196368618988));
#12165=CARTESIAN_POINT('Ctrl Pts',(-21.6377126842389,20.9492978854477,-62.4954659659575));
#12166=CARTESIAN_POINT('Ctrl Pts',(-21.4865842941244,21.0674988789648,-62.4825520171268));
#12167=CARTESIAN_POINT('Ctrl Pts',(-21.3380995147647,21.2066143843359,-62.4697238008891));
#12168=CARTESIAN_POINT('Ctrl Pts',(-21.329413080806,21.2148440277814,-62.4689728702153));
#12169=CARTESIAN_POINT('Ctrl Pts',(-21.3182063534283,21.2255805010668,-62.4680036877972));
#12170=CARTESIAN_POINT('Ctrl Pts',(-21.3156442373354,21.2280432467748,-62.4677820846919));
#12171=CARTESIAN_POINT('Ctrl Pts',(-21.3117206938662,21.2318271237327,-62.4674426968128));
#12172=CARTESIAN_POINT('Ctrl Pts',(-21.3103563611794,21.2331452172593,-62.4673246756239));
#12173=CARTESIAN_POINT('Ctrl Pts',(-21.3076815727431,21.2357339233669,-62.467093283669));
#12174=CARTESIAN_POINT('Ctrl Pts',(-21.3063710394377,21.2370044380026,-62.4669799067896));
#12175=CARTESIAN_POINT('Ctrl Pts',(-21.3034724343946,21.2398193117493,-62.4667291319475));
#12176=CARTESIAN_POINT('Ctrl Pts',(-21.3018848791402,21.2413641912875,-62.4665917761338));
#12177=CARTESIAN_POINT('Ctrl Pts',(-21.2985906646526,21.2445764720802,-62.4663067410332));
#12178=CARTESIAN_POINT('Ctrl Pts',(-21.2968842608815,21.2462441351061,-62.4661590824181));
#12179=CARTESIAN_POINT('Ctrl Pts',(-21.2925027960438,21.250535650393,-62.4657799135583));
#12180=CARTESIAN_POINT('Ctrl Pts',(-21.2898304468607,21.2531622849469,-62.465548619879));
#12181=CARTESIAN_POINT('Ctrl Pts',(-21.2820798459959,21.2608069221761,-62.4648776892639));
#12182=CARTESIAN_POINT('Ctrl Pts',(-21.2770136399607,21.2658371853876,-62.4644389946543));
#12183=CARTESIAN_POINT('Ctrl Pts',(-21.225252969352,21.3175733346556,-62.4599549544061));
#12184=CARTESIAN_POINT('Ctrl Pts',(-21.1799841410761,21.3656911221856,-62.4560168016529));
#12185=CARTESIAN_POINT('Ctrl Pts',(-21.1073131894992,21.4478564954779,-62.4495980669304));
#12186=CARTESIAN_POINT('Ctrl Pts',(-21.0790695146452,21.4811279588523,-62.4470771215526));
#12187=CARTESIAN_POINT('Ctrl Pts',(-20.8888330353287,21.7146831006293,-62.4298317892197));
#12188=CARTESIAN_POINT('Ctrl Pts',(-20.7506852694502,21.9331861954486,-62.4158578580381));
#12189=CARTESIAN_POINT('Ctrl Pts',(-20.62290290992,22.2017980281518,-62.398784580381));
#12190=CARTESIAN_POINT('Ctrl Pts',(-20.6064545648679,22.2380944901982,-62.3964816131576));
#12191=CARTESIAN_POINT('Ctrl Pts',(-20.5527229282712,22.362762572066,-62.3885696984649));
#12192=CARTESIAN_POINT('Ctrl Pts',(-20.5187159551936,22.4524823688718,-62.3828707710595));
#12193=CARTESIAN_POINT('Ctrl Pts',(-20.4855833666699,22.5532450029337,-62.3764141911182));
#12194=CARTESIAN_POINT('Ctrl Pts',(-20.4824507232505,22.5629262614915,-62.3757933044682));
#12195=CARTESIAN_POINT('Ctrl Pts',(-20.4780965779661,22.5766033059459,-62.3749153439588));
#12196=CARTESIAN_POINT('Ctrl Pts',(-20.4768368943547,22.5805869508278,-62.3746595278012));
#12197=CARTESIAN_POINT('Ctrl Pts',(-20.4746475289468,22.587557763318,-62.3742117121664));
#12198=CARTESIAN_POINT('Ctrl Pts',(-20.4737144414339,22.5905438628492,-62.3740198249163));
#12199=CARTESIAN_POINT('Ctrl Pts',(-20.4717655999712,22.596812663837,-62.3736168719164));
#12200=CARTESIAN_POINT('Ctrl Pts',(-20.4707507458951,22.6000956385834,-62.3734057769158));
#12201=CARTESIAN_POINT('Ctrl Pts',(-20.4683438675013,22.6079260674626,-62.372902115283));
#12202=CARTESIAN_POINT('Ctrl Pts',(-20.4669566575854,22.6124749824137,-62.372609391081));
#12203=CARTESIAN_POINT('Ctrl Pts',(-20.4623231982198,22.6277903649141,-62.371623382792));
#12204=CARTESIAN_POINT('Ctrl Pts',(-20.4591232605465,22.6385706564883,-62.3709285834063));
#12205=CARTESIAN_POINT('Ctrl Pts',(-20.4517050611124,22.6640499659495,-62.3692845333739));
#12206=CARTESIAN_POINT('Ctrl Pts',(-20.4475349009567,22.678762597222,-62.3683337259384));
#12207=CARTESIAN_POINT('Ctrl Pts',(-20.4019687158948,22.8439969248488,-62.357637976271));
#12208=CARTESIAN_POINT('Ctrl Pts',(-20.3714635190606,22.9972828950226,-62.3475381313239));
#12209=CARTESIAN_POINT('Ctrl Pts',(-20.3145754926392,23.4542873862186,-62.3169605771201));
#12210=CARTESIAN_POINT('Ctrl Pts',(-20.3199697832875,23.7601993605823,-62.2957649898941));
#12211=CARTESIAN_POINT('Ctrl Pts',(-20.3735452612076,24.094115562082,-62.2740722363186));
#12212=CARTESIAN_POINT('Ctrl Pts',(-20.3794138030826,24.1273470298568,-62.2719317116986));
#12213=CARTESIAN_POINT('Ctrl Pts',(-20.3867635442163,24.1654603800735,-62.2695026387098));
#12214=CARTESIAN_POINT('Ctrl Pts',(-20.387735366568,24.170436739588,-62.2691859912817));
#12215=CARTESIAN_POINT('Ctrl Pts',(-20.3891849250557,24.1777674075226,-62.268720311754));
#12216=CARTESIAN_POINT('Ctrl Pts',(-20.3896535496831,24.1801234773057,-62.2685707606277));
#12217=CARTESIAN_POINT('Ctrl Pts',(-20.3904851010615,24.1842799126488,-62.2683071422649));
#12218=CARTESIAN_POINT('Ctrl Pts',(-20.3908469324937,24.1860804921485,-62.2681930119205));
#12219=CARTESIAN_POINT('Ctrl Pts',(-20.3916101862663,24.1898619289431,-62.2679534719484));
#12220=CARTESIAN_POINT('Ctrl Pts',(-20.3920119319689,24.1918427137264,-62.2678280814847));
#12221=CARTESIAN_POINT('Ctrl Pts',(-20.3930629121485,24.1969996057856,-62.2675018505547));
#12222=CARTESIAN_POINT('Ctrl Pts',(-20.3937150780703,24.2001751237792,-62.2673011790571));
#12223=CARTESIAN_POINT('Ctrl Pts',(-20.3951500869177,24.2071093394906,-62.2668634430012));
#12224=CARTESIAN_POINT('Ctrl Pts',(-20.395934858629,24.2108676395523,-62.2666264883575));
#12225=CARTESIAN_POINT('Ctrl Pts',(-20.3982482684929,24.2218485333336,-62.2659350011615));
#12226=CARTESIAN_POINT('Ctrl Pts',(-20.3997950230051,24.2290673467031,-62.2654814822521));
#12227=CARTESIAN_POINT('Ctrl Pts',(-20.4051890310656,24.2538259687478,-62.2639294849665));
#12228=CARTESIAN_POINT('Ctrl Pts',(-20.4091581444798,24.2713392727152,-62.2628376167247));
#12229=CARTESIAN_POINT('Ctrl Pts',(-20.4258643510753,24.3422970350845,-62.2584345878878));
#12230=CARTESIAN_POINT('Ctrl Pts',(-20.4398214303909,24.3954478476165,-62.2551846048492));
#12231=CARTESIAN_POINT('Ctrl Pts',(-20.4776536665992,24.525848425691,-62.2472723473582));
#12232=CARTESIAN_POINT('Ctrl Pts',(-20.5030896406238,24.6026074511085,-62.2426685708219));
#12233=CARTESIAN_POINT('Ctrl Pts',(-20.6079656375818,24.8832671449607,-62.2257718633631));
#12234=CARTESIAN_POINT('Ctrl Pts',(-20.7052102531172,25.0798649597946,-62.2137677123514));
#12235=CARTESIAN_POINT('Ctrl Pts',(-20.8496149533322,25.3096393451987,-62.1981586879506));
#12236=CARTESIAN_POINT('Ctrl Pts',(-20.8786940365292,25.3534885415055,-62.1951043679517));
#12237=CARTESIAN_POINT('Ctrl Pts',(-20.913766832805,25.4036642251259,-62.1915083867524));
#12238=CARTESIAN_POINT('Ctrl Pts',(-20.9187295560934,25.4107037062092,-62.1910015216658));
#12239=CARTESIAN_POINT('Ctrl Pts',(-20.9642648937927,25.4747475659943,-62.186368210173));
#12240=CARTESIAN_POINT('Ctrl Pts',(-21.0066530898595,25.5304328140481,-62.1821797817258));
#12241=CARTESIAN_POINT('Ctrl Pts',(-21.0568005760059,25.59204212293,-62.1773414108091));
#12242=CARTESIAN_POINT('Ctrl Pts',(-21.0628159796526,25.5993661905116,-62.1767628502344));
#12243=CARTESIAN_POINT('Ctrl Pts',(-21.071662583856,25.6100410341644,-62.1759145927527));
#12244=CARTESIAN_POINT('Ctrl Pts',(-21.0744684963369,25.6134127810209,-62.1756459274161));
#12245=CARTESIAN_POINT('Ctrl Pts',(-21.0794526500611,25.6193772196267,-62.175169362533));
#12246=CARTESIAN_POINT('Ctrl Pts',(-21.0816281145247,25.6219722318721,-62.1749615768943));
#12247=CARTESIAN_POINT('Ctrl Pts',(-21.0861538267782,25.6273534974236,-62.1745297723094));
#12248=CARTESIAN_POINT('Ctrl Pts',(-21.0885047187776,25.6301392004407,-62.1743057270604));
#12249=CARTESIAN_POINT('Ctrl Pts',(-21.0945761019469,25.6373088068375,-62.1737277670591));
#12250=CARTESIAN_POINT('Ctrl Pts',(-21.0983035966248,25.6416867387296,-62.1733735638283));
#12251=CARTESIAN_POINT('Ctrl Pts',(-21.1138835344393,25.659886432085,-62.1718956915996));
#12252=CARTESIAN_POINT('Ctrl Pts',(-21.1258411064956,25.6736173858656,-62.1707676704235));
#12253=CARTESIAN_POINT('Ctrl Pts',(-21.3403937089623,25.915814408338,-62.1506348921258));
#12254=CARTESIAN_POINT('Ctrl Pts',(-21.5742867367526,26.1143953877523,-62.1301401747579));
#12255=CARTESIAN_POINT('Ctrl Pts',(-21.911347402691,26.3267224712512,-62.1031866758546));
#12256=CARTESIAN_POINT('Ctrl Pts',(-21.9922607439807,26.3729192105752,-62.096902306304));
#12257=CARTESIAN_POINT('Ctrl Pts',(-22.0750361387181,26.4155368380754,-62.0907209741597));
#12258=CARTESIAN_POINT('Origin',(-23.5502525316942,23.5502525316942,-77.3107734492734));
#12259=CARTESIAN_POINT('',(-22.0750360153461,26.4155367745563,-60.593221446491));
#12260=CARTESIAN_POINT('',(-22.0750360359093,26.4155367851434,-60.8417499040898));
#12261=CARTESIAN_POINT('',(-22.0750360153461,26.4155367745563,-77.3107734492734));
#12262=CARTESIAN_POINT('',(-26.7730010715128,23.5532478318311,-61.4389926964188));
#12263=CARTESIAN_POINT('Ctrl Pts',(-22.0750360153461,26.4155367745563,-60.593221446491));
#12264=CARTESIAN_POINT('Ctrl Pts',(-22.0629295894779,26.4093036758893,-60.5940645766529));
#12265=CARTESIAN_POINT('Ctrl Pts',(-22.0508629408241,26.4029939895318,-60.5949104149417));
#12266=CARTESIAN_POINT('Ctrl Pts',(-21.9245463063757,26.3359198149904,-60.6038232154706));
#12267=CARTESIAN_POINT('Ctrl Pts',(-21.8140296098913,26.2684109826019,-60.6121320731002));
#12268=CARTESIAN_POINT('Ctrl Pts',(-21.5224687497516,26.0652629397668,-60.6355076782888));
#12269=CARTESIAN_POINT('Ctrl Pts',(-21.3511692352329,25.9169379138015,-60.650966190823));
#12270=CARTESIAN_POINT('Ctrl Pts',(-21.1031706140023,25.6518461502569,-60.6753493770457));
#12271=CARTESIAN_POINT('Ctrl Pts',(-21.0159966639256,25.5458634344544,-60.6844124721604));
#12272=CARTESIAN_POINT('Ctrl Pts',(-20.9311370733983,25.4281279704951,-60.6935268065851));
#12273=CARTESIAN_POINT('Ctrl Pts',(-20.926469584239,25.4216009747837,-60.6940291278711));
#12274=CARTESIAN_POINT('Ctrl Pts',(-20.9202517003813,25.4128369180658,-60.6946995890625));
#12275=CARTESIAN_POINT('Ctrl Pts',(-20.9186797436697,25.4106153002215,-60.6948692007127));
#12276=CARTESIAN_POINT('Ctrl Pts',(-20.9160456183733,25.4068825196206,-60.6951536014764));
#12277=CARTESIAN_POINT('Ctrl Pts',(-20.9149819351257,25.4053724354086,-60.695268495286));
#12278=CARTESIAN_POINT('Ctrl Pts',(-20.9129511920751,25.4024841697756,-60.6954879409646));
#12279=CARTESIAN_POINT('Ctrl Pts',(-20.9119839199713,25.4011061535354,-60.6955925071926));
#12280=CARTESIAN_POINT('Ctrl Pts',(-20.9097101404225,25.3978614280526,-60.6958384099497));
#12281=CARTESIAN_POINT('Ctrl Pts',(-20.9084045341484,25.3959940932206,-60.6959796837129));
#12282=CARTESIAN_POINT('Ctrl Pts',(-20.9046694319182,25.3906399053715,-60.6963840657479));
#12283=CARTESIAN_POINT('Ctrl Pts',(-20.9022448394864,25.3871496125106,-60.696646836774));
#12284=CARTESIAN_POINT('Ctrl Pts',(-20.886875711018,25.3649315017008,-60.6983143057626));
#12285=CARTESIAN_POINT('Ctrl Pts',(-20.8741225976182,25.3460711470696,-60.6997061124847));
#12286=CARTESIAN_POINT('Ctrl Pts',(-20.8354468811579,25.2875472190912,-60.7039577552958));
#12287=CARTESIAN_POINT('Ctrl Pts',(-20.8101971841859,25.2474442585395,-60.7067774464783));
#12288=CARTESIAN_POINT('Ctrl Pts',(-20.745982161243,25.1402833233576,-60.7141085625629));
#12289=CARTESIAN_POINT('Ctrl Pts',(-20.7085357391707,25.0723488908379,-60.7185524641844));
#12290=CARTESIAN_POINT('Ctrl Pts',(-20.5831671367227,24.8241200496182,-60.7343043373909));
#12291=CARTESIAN_POINT('Ctrl Pts',(-20.5096652381694,24.6370670185044,-60.7453120516262));
#12292=CARTESIAN_POINT('Ctrl Pts',(-20.4335546049344,24.3735111861286,-60.760915465919));
#12293=CARTESIAN_POINT('Ctrl Pts',(-20.4155261811194,24.3019509660849,-60.7651574480202));
#12294=CARTESIAN_POINT('Ctrl Pts',(-20.3943309265492,24.2036983724629,-60.7710303546979));
#12295=CARTESIAN_POINT('Ctrl Pts',(-20.38901769181,24.1774900264102,-60.7726014940135));
#12296=CARTESIAN_POINT('Ctrl Pts',(-20.3831329153975,24.1464857997032,-60.7744668933887));
#12297=CARTESIAN_POINT('Ctrl Pts',(-20.3822451259872,24.1417505036741,-60.7747519820622));
#12298=CARTESIAN_POINT('Ctrl Pts',(-20.3806294730297,24.1330249405093,-60.7752776570649));
#12299=CARTESIAN_POINT('Ctrl Pts',(-20.3798985171012,24.1290352512332,-60.7755181529275));
#12300=CARTESIAN_POINT('Ctrl Pts',(-20.3781239373979,24.1192450439116,-60.776108641344));
#12301=CARTESIAN_POINT('Ctrl Pts',(-20.3770886923592,24.1134430374665,-60.7764588781737));
#12302=CARTESIAN_POINT('Ctrl Pts',(-20.3748745787056,24.1008341707082,-60.7772206705075));
#12303=CARTESIAN_POINT('Ctrl Pts',(-20.373701671383,24.0940263048094,-60.7776324005006));
#12304=CARTESIAN_POINT('Ctrl Pts',(-20.3708201829052,24.0769738738393,-60.7786647948808));
#12305=CARTESIAN_POINT('Ctrl Pts',(-20.3691392277362,24.0667247734084,-60.7792862813563));
#12306=CARTESIAN_POINT('Ctrl Pts',(-20.3658750062327,24.0462015218124,-60.780532844986));
#12307=CARTESIAN_POINT('Ctrl Pts',(-20.3642918500155,24.0359274810758,-60.7811579173184));
#12308=CARTESIAN_POINT('Ctrl Pts',(-20.3589085871458,23.9998329238091,-60.7833577236261));
#12309=CARTESIAN_POINT('Ctrl Pts',(-20.3553725256304,23.9739745942572,-60.7849405306397));
#12310=CARTESIAN_POINT('Ctrl Pts',(-20.3513127771927,23.9413383510584,-60.7869477280901));
#12311=CARTESIAN_POINT('Ctrl Pts',(-20.3504958663733,23.9345973673013,-60.7873628220553));
#12312=CARTESIAN_POINT('Ctrl Pts',(-20.3492412002901,23.9239628071937,-60.788018493201));
#12313=CARTESIAN_POINT('Ctrl Pts',(-20.3487892276922,23.9200709015794,-60.78825862069));
#12314=CARTESIAN_POINT('Ctrl Pts',(-20.3480028588396,23.91319004814,-60.7886834731396));
#12315=CARTESIAN_POINT('Ctrl Pts',(-20.3476655466704,23.9102014327875,-60.7888681057238));
#12316=CARTESIAN_POINT('Ctrl Pts',(-20.3469020267589,23.9033505406097,-60.7892915826724));
#12317=CARTESIAN_POINT('Ctrl Pts',(-20.3464786202626,23.8994879617272,-60.7895305152386));
#12318=CARTESIAN_POINT('Ctrl Pts',(-20.3453450091759,23.8889708829131,-60.7901815607649));
#12319=CARTESIAN_POINT('Ctrl Pts',(-20.3446485481271,23.8823149487245,-60.7905941069407));
#12320=CARTESIAN_POINT('Ctrl Pts',(-20.3411282000235,23.8476282001323,-60.7927468019594));
#12321=CARTESIAN_POINT('Ctrl Pts',(-20.3386513029664,23.819564118298,-60.7944978587341));
#12322=CARTESIAN_POINT('Ctrl Pts',(-20.3293711352232,23.6959265759748,-60.802255700593));
#12323=CARTESIAN_POINT('Ctrl Pts',(-20.3264646614019,23.6001180544829,-60.8083835997558));
#12324=CARTESIAN_POINT('Ctrl Pts',(-20.3307555862706,23.299021115464,-60.8280155815751));
#12325=CARTESIAN_POINT('Ctrl Pts',(-20.3532957588069,23.0944815410163,-60.8419331950849));
#12326=CARTESIAN_POINT('Ctrl Pts',(-20.4243873970138,22.7529464204359,-60.8655247859126));
#12327=CARTESIAN_POINT('Ctrl Pts',(-20.4630074539174,22.6144880307889,-60.8751785135582));
#12328=CARTESIAN_POINT('Ctrl Pts',(-20.51114708899,22.4778919603597,-60.8845255697523));
#12329=CARTESIAN_POINT('Ctrl Pts',(-20.5115581342842,22.4767277550888,-60.8846052207176));
#12330=CARTESIAN_POINT('Ctrl Pts',(-20.5129775313339,22.4727149379016,-60.8848797158078));
#12331=CARTESIAN_POINT('Ctrl Pts',(-20.5139892237836,22.4698674989269,-60.8850744098931));
#12332=CARTESIAN_POINT('Ctrl Pts',(-20.5280681914919,22.4304177870292,-60.8877705881564));
#12333=CARTESIAN_POINT('Ctrl Pts',(-20.541793271899,22.3940513115643,-60.8902417167156));
#12334=CARTESIAN_POINT('Ctrl Pts',(-20.558103281076,22.3530943847891,-60.8930012852786));
#12335=CARTESIAN_POINT('Ctrl Pts',(-20.5600447199996,22.3482533592871,-60.8933270848033));
#12336=CARTESIAN_POINT('Ctrl Pts',(-20.5629218554541,22.3411292622027,-60.8938059572501));
#12337=CARTESIAN_POINT('Ctrl Pts',(-20.5638484224314,22.3388425489439,-60.8939595793608));
#12338=CARTESIAN_POINT('Ctrl Pts',(-20.5654889849204,22.3348070576742,-60.8942305270103));
#12339=CARTESIAN_POINT('Ctrl Pts',(-20.5662018924274,22.3330578419129,-60.8943479189146));
#12340=CARTESIAN_POINT('Ctrl Pts',(-20.5676892680153,22.3294175237322,-60.894592114428));
#12341=CARTESIAN_POINT('Ctrl Pts',(-20.5684639954639,22.3275265346802,-60.8947189016522));
#12342=CARTESIAN_POINT('Ctrl Pts',(-20.5704825861371,22.3226127969967,-60.8950482007449));
#12343=CARTESIAN_POINT('Ctrl Pts',(-20.5717292543393,22.3195911919527,-60.8952505414041));
#12344=CARTESIAN_POINT('Ctrl Pts',(-20.5769812275217,22.3069164794498,-60.8960986678618));
#12345=CARTESIAN_POINT('Ctrl Pts',(-20.5810289376823,22.2972808468995,-60.8967418970492));
#12346=CARTESIAN_POINT('Ctrl Pts',(-20.6403727627809,22.1579145993769,-60.9060253789512));
#12347=CARTESIAN_POINT('Ctrl Pts',(-20.7040871932893,22.0319116088658,-60.9141700836784));
#12348=CARTESIAN_POINT('Ctrl Pts',(-20.8559633228212,21.7749478338147,-60.9310674744833));
#12349=CARTESIAN_POINT('Ctrl Pts',(-20.9458884404335,21.6454715007117,-60.9397637518679));
#12350=CARTESIAN_POINT('Ctrl Pts',(-21.1714834303234,21.3666634326872,-60.9599521380771));
#12351=CARTESIAN_POINT('Ctrl Pts',(-21.3123987992193,21.2224647367113,-60.9715234793257));
#12352=CARTESIAN_POINT('Ctrl Pts',(-21.4754453898374,21.0841924984787,-60.9845141646886));
#12353=CARTESIAN_POINT('Ctrl Pts',(-21.4851161151597,21.0760883622566,-60.9852831642865));
#12354=CARTESIAN_POINT('Ctrl Pts',(-21.4983942245457,21.0650932982952,-60.9863370608412));
#12355=CARTESIAN_POINT('Ctrl Pts',(-21.5019606977756,21.0621529575808,-60.9866199440364));
#12356=CARTESIAN_POINT('Ctrl Pts',(-21.5080415903055,21.0571615661509,-60.9871019449916));
#12357=CARTESIAN_POINT('Ctrl Pts',(-21.5105528118186,21.0551066152746,-60.9873009042595));
#12358=CARTESIAN_POINT('Ctrl Pts',(-21.5154160511688,21.0511392390645,-60.9876860332429));
#12359=CARTESIAN_POINT('Ctrl Pts',(-21.5177676726888,21.049226332373,-60.9878721831455));
#12360=CARTESIAN_POINT('Ctrl Pts',(-21.5233544257301,21.0446949184609,-60.9883142338457));
#12361=CARTESIAN_POINT('Ctrl Pts',(-21.5265919318267,21.0420793595474,-60.9885702532075));
#12362=CARTESIAN_POINT('Ctrl Pts',(-21.5360305710426,21.0344841188369,-60.9893162304157));
#12363=CARTESIAN_POINT('Ctrl Pts',(-21.5422450487759,21.029521137708,-60.9898068585601));
#12364=CARTESIAN_POINT('Ctrl Pts',(-21.5886479881317,20.992743496649,-60.9934665112024));
#12365=CARTESIAN_POINT('Ctrl Pts',(-21.6295700144874,20.961870212821,-60.9966728136921));
#12366=CARTESIAN_POINT('Ctrl Pts',(-21.724037803362,20.8940737648434,-61.004033352073));
#12367=CARTESIAN_POINT('Ctrl Pts',(-21.7779987051726,20.8577701649321,-61.0082092463986));
#12368=CARTESIAN_POINT('Ctrl Pts',(-21.9847947371882,20.7275535247361,-61.0241081105888));
#12369=CARTESIAN_POINT('Ctrl Pts',(-22.1442694589494,20.6448289665185,-61.0361842092896));
#12370=CARTESIAN_POINT('Ctrl Pts',(-22.4442066273927,20.5197419291131,-61.0581816837083));
#12371=CARTESIAN_POINT('Ctrl Pts',(-22.5822904639535,20.4728532338643,-61.0680499798475));
#12372=CARTESIAN_POINT('Ctrl Pts',(-22.7454260943733,20.4295304106614,-61.079118871065));
#12373=CARTESIAN_POINT('Ctrl Pts',(-22.7678365076605,20.4238364730539,-61.0806266482866));
#12374=CARTESIAN_POINT('Ctrl Pts',(-22.7950477614833,20.4172336812214,-61.0824404699813));
#12375=CARTESIAN_POINT('Ctrl Pts',(-22.7997913328638,20.4160940558048,-61.0827560405774));
#12376=CARTESIAN_POINT('Ctrl Pts',(-22.8087635021778,20.4139600627138,-61.0833517250838));
#12377=CARTESIAN_POINT('Ctrl Pts',(-22.8129915535108,20.4129634659019,-61.0836319338836));
#12378=CARTESIAN_POINT('Ctrl Pts',(-22.856230382667,20.4028638485818,-61.0864923171289));
#12379=CARTESIAN_POINT('Ctrl Pts',(-22.8954079154917,20.3944798587892,-61.0890406861707));
#12380=CARTESIAN_POINT('Ctrl Pts',(-22.9399643842328,20.3858103478716,-61.0918822333915));
#12381=CARTESIAN_POINT('Ctrl Pts',(-22.9451975657881,20.3848055732236,-61.0922150921786));
#12382=CARTESIAN_POINT('Ctrl Pts',(-22.9528418891064,20.3833575071793,-61.0927000006252));
#12383=CARTESIAN_POINT('Ctrl Pts',(-22.9552510477401,20.3829039865601,-61.0928526326061));
#12384=CARTESIAN_POINT('Ctrl Pts',(-22.9595149986235,20.3821063405991,-61.093122435575));
#12385=CARTESIAN_POINT('Ctrl Pts',(-22.9613695767238,20.3817610946617,-61.0932396711037));
#12386=CARTESIAN_POINT('Ctrl Pts',(-22.9652409277355,20.381043925216,-61.0934841571537));
#12387=CARTESIAN_POINT('Ctrl Pts',(-22.9672577485344,20.3806722990755,-61.0936113902451));
#12388=CARTESIAN_POINT('Ctrl Pts',(-22.9725218736428,20.3797075081967,-61.0939431350412));
#12389=CARTESIAN_POINT('Ctrl Pts',(-22.9757697475294,20.3791174052438,-61.0941474707479));
#12390=CARTESIAN_POINT('Ctrl Pts',(-22.9896116612382,20.376624445265,-61.0950168687151));
#12391=CARTESIAN_POINT('Ctrl Pts',(-23.0002144515361,20.3747696495597,-61.0956792085634));
#12392=CARTESIAN_POINT('Ctrl Pts',(-23.107764701046,20.3565102201632,-61.1023629530546));
#12393=CARTESIAN_POINT('Ctrl Pts',(-23.2054163680483,20.3444955641927,-61.1081460954601));
#12394=CARTESIAN_POINT('Ctrl Pts',(-23.4659661721426,20.3244855566878,-61.1231814455632));
#12395=CARTESIAN_POINT('Ctrl Pts',(-23.6291788038445,20.3243490468427,-61.1322023952955));
#12396=CARTESIAN_POINT('Ctrl Pts',(-24.026524373483,20.3542030399277,-61.1545053321937));
#12397=CARTESIAN_POINT('Ctrl Pts',(-24.2586590555303,20.3975230135828,-61.1678755418505));
#12398=CARTESIAN_POINT('Ctrl Pts',(-24.4978796027487,20.4699390461666,-61.1830446851712));
#12399=CARTESIAN_POINT('Ctrl Pts',(-24.5117428486926,20.4742381308088,-61.1839286100201));
#12400=CARTESIAN_POINT('Ctrl Pts',(-24.5307680742237,20.4802791597701,-61.1851484985942));
#12401=CARTESIAN_POINT('Ctrl Pts',(-24.5359555296671,20.4819408081766,-61.1854818170897));
#12402=CARTESIAN_POINT('Ctrl Pts',(-24.5442031436713,20.4846057623215,-61.1860128906703));
#12403=CARTESIAN_POINT('Ctrl Pts',(-24.5472660701397,20.4856005224688,-61.1862103635405));
#12404=CARTESIAN_POINT('Ctrl Pts',(-24.5532171079751,20.4875431329991,-61.1865945219092));
#12405=CARTESIAN_POINT('Ctrl Pts',(-24.5561053806212,20.4884904820996,-61.1867811906827));
#12406=CARTESIAN_POINT('Ctrl Pts',(-24.563002620158,20.4907635792258,-61.1872274903984));
#12407=CARTESIAN_POINT('Ctrl Pts',(-24.5670103225148,20.4920931201375,-61.1874872465629));
#12408=CARTESIAN_POINT('Ctrl Pts',(-24.5753152254349,20.4948663717017,-61.1880264189107));
#12409=CARTESIAN_POINT('Ctrl Pts',(-24.5796120136838,20.4963112799224,-61.188305874348));
#12410=CARTESIAN_POINT('Ctrl Pts',(-24.6045625642876,20.5047601983882,-61.1899315286279));
#12411=CARTESIAN_POINT('Ctrl Pts',(-24.6251474483064,20.5119645141368,-61.1912843623856));
#12412=CARTESIAN_POINT('Ctrl Pts',(-24.6792509436818,20.5315183438682,-61.1948714763877));
#12413=CARTESIAN_POINT('Ctrl Pts',(-24.712639335826,20.5442168926455,-61.1971172836032));
#12414=CARTESIAN_POINT('Ctrl Pts',(-24.8652815766188,20.6051943319239,-61.2075364452174));
#12415=CARTESIAN_POINT('Ctrl Pts',(-24.9817751779936,20.6600267330605,-61.2159261283969));
#12416=CARTESIAN_POINT('Ctrl Pts',(-25.1777375010472,20.7670228161099,-61.2307784254913));
#12417=CARTESIAN_POINT('Ctrl Pts',(-25.2587638024771,20.8160135558481,-61.2371556158962));
#12418=CARTESIAN_POINT('Ctrl Pts',(-25.4517457494089,20.9446267109967,-61.2528425305402));
#12419=CARTESIAN_POINT('Ctrl Pts',(-25.5610006206194,21.0279803308805,-61.2621671343419));
#12420=CARTESIAN_POINT('Ctrl Pts',(-25.6850094812523,21.135783447527,-61.273065322758));
#12421=CARTESIAN_POINT('Ctrl Pts',(-25.705185696925,21.1537735897954,-61.2748489207406));
#12422=CARTESIAN_POINT('Ctrl Pts',(-25.735113309361,21.1811421865984,-61.277507565198));
#12423=CARTESIAN_POINT('Ctrl Pts',(-25.7450355477209,21.1903313532693,-61.2783912096354));
#12424=CARTESIAN_POINT('Ctrl Pts',(-25.7573989442393,21.2019267417477,-61.2794947113276));
#12425=CARTESIAN_POINT('Ctrl Pts',(-25.7598943651635,21.2042746396173,-61.2797175679266));
#12426=CARTESIAN_POINT('Ctrl Pts',(-25.7680284083514,21.2119523106597,-61.2804443885856));
#12427=CARTESIAN_POINT('Ctrl Pts',(-25.773651571312,21.2172985082201,-61.2809474779172));
#12428=CARTESIAN_POINT('Ctrl Pts',(-25.784303759794,21.2274995248182,-61.2819016100655));
#12429=CARTESIAN_POINT('Ctrl Pts',(-25.7893363980963,21.2323504928552,-61.2823528661239));
#12430=CARTESIAN_POINT('Ctrl Pts',(-25.8230885540194,21.2650967537914,-61.2853822528281));
#12431=CARTESIAN_POINT('Ctrl Pts',(-25.8513035190106,21.2935103587043,-61.2879292058016));
#12432=CARTESIAN_POINT('Ctrl Pts',(-25.8826662480234,21.326293852951,-61.2907693285691));
#12433=CARTESIAN_POINT('Ctrl Pts',(-25.8863397652418,21.3301528971949,-61.2911021354831));
#12434=CARTESIAN_POINT('Ctrl Pts',(-25.8916894505121,21.335800742513,-61.2915869825293));
#12435=CARTESIAN_POINT('Ctrl Pts',(-25.8933731499115,21.3375823484106,-61.291739604775));
#12436=CARTESIAN_POINT('Ctrl Pts',(-25.8963489450772,21.3407383904971,-61.2920093965138));
#12437=CARTESIAN_POINT('Ctrl Pts',(-25.8976418676301,21.3421120409991,-61.2921266305294));
#12438=CARTESIAN_POINT('Ctrl Pts',(-25.9003378963796,21.3449814492349,-61.2923711195549));
#12439=CARTESIAN_POINT('Ctrl Pts',(-25.9017407781476,21.3464774081192,-61.2924983571245));
#12440=CARTESIAN_POINT('Ctrl Pts',(-25.905398226174,21.3503849858643,-61.2928301264722));
#12441=CARTESIAN_POINT('Ctrl Pts',(-25.9076505237505,21.3527987395285,-61.2930344822036));
#12442=CARTESIAN_POINT('Ctrl Pts',(-25.9125390555374,21.3580538717288,-61.2934781458086));
#12443=CARTESIAN_POINT('Ctrl Pts',(-25.9151738851315,21.3608965583744,-61.2937173465585));
#12444=CARTESIAN_POINT('Ctrl Pts',(-25.9489770999678,21.3974986737711,-61.2967872053593));
#12445=CARTESIAN_POINT('Ctrl Pts',(-25.9794271535135,21.4319182997606,-61.2995641939224));
#12446=CARTESIAN_POINT('Ctrl Pts',(-26.0851323930585,21.5566818322005,-61.3092964105691));
#12447=CARTESIAN_POINT('Ctrl Pts',(-26.156174067329,21.6504846087297,-61.3160124975595));
#12448=CARTESIAN_POINT('Ctrl Pts',(-26.2473623310464,21.7856609229995,-61.3252023900886));
#12449=CARTESIAN_POINT('Ctrl Pts',(-26.2719890418996,21.8238877717852,-61.3277503093511));
#12450=CARTESIAN_POINT('Ctrl Pts',(-26.3205902575429,21.9029554312564,-61.3329417979302));
#12451=CARTESIAN_POINT('Ctrl Pts',(-26.344489851636,21.9438289698151,-61.3355843374131));
#12452=CARTESIAN_POINT('Ctrl Pts',(-26.4866582221311,22.1997464591655,-61.3519539813876));
#12453=CARTESIAN_POINT('Ctrl Pts',(-26.5809232315095,22.4271518197624,-61.3658275944521));
#12454=CARTESIAN_POINT('Ctrl Pts',(-26.6500132423966,22.6684178103628,-61.3810450432634));
#12455=CARTESIAN_POINT('Ctrl Pts',(-26.6515412810313,22.6738068505595,-61.3813851469759));
#12456=CARTESIAN_POINT('Ctrl Pts',(-26.656250004848,22.6905799354696,-61.3824443404705));
#12457=CARTESIAN_POINT('Ctrl Pts',(-26.6593820888514,22.7019774189456,-61.383164989052));
#12458=CARTESIAN_POINT('Ctrl Pts',(-26.6636188152573,22.7177333671218,-61.3841625624633));
#12459=CARTESIAN_POINT('Ctrl Pts',(-26.6647771699699,22.722077397892,-61.3844377414432));
#12460=CARTESIAN_POINT('Ctrl Pts',(-26.6667471228288,22.7295276489118,-61.3849099346824));
#12461=CARTESIAN_POINT('Ctrl Pts',(-26.6675631785666,22.7326326930321,-61.3851068040504));
#12462=CARTESIAN_POINT('Ctrl Pts',(-26.6691438171135,22.7386836957279,-61.3854906009021));
#12463=CARTESIAN_POINT('Ctrl Pts',(-26.6699088692646,22.7416295285972,-61.3856775128954));
#12464=CARTESIAN_POINT('Ctrl Pts',(-26.6717320029493,22.7486906015808,-61.3861256972143));
#12465=CARTESIAN_POINT('Ctrl Pts',(-26.6727861188989,22.7528068509272,-61.3863870976995));
#12466=CARTESIAN_POINT('Ctrl Pts',(-26.6749570651585,22.7613545496068,-61.3869301931893));
#12467=CARTESIAN_POINT('Ctrl Pts',(-26.6760726155802,22.7657863116293,-61.3872119290437));
#12468=CARTESIAN_POINT('Ctrl Pts',(-26.6789693141251,22.7773983495921,-61.3879505415985));
#12469=CARTESIAN_POINT('Ctrl Pts',(-26.680735164004,22.7845823815649,-61.3884079123157));
#12470=CARTESIAN_POINT('Ctrl Pts',(-26.7428652624061,23.0411551712546,-61.4047576911774));
#12471=CARTESIAN_POINT('Ctrl Pts',(-26.773239550744,23.2967895314256,-61.4216706112496));
#12472=CARTESIAN_POINT('Ctrl Pts',(-26.7730011391294,23.5532484913554,-61.4389926226415));
#12473=CARTESIAN_POINT('Ctrl Pts',(-26.773001139735,23.5532478398496,-61.4389925786368));
#12474=CARTESIAN_POINT('Ctrl Pts',(-26.7727947908402,23.7752652681641,-61.4539883047879));
#12475=CARTESIAN_POINT('Ctrl Pts',(-26.7496469772921,23.9966896922317,-61.4691737663365));
#12476=CARTESIAN_POINT('Ctrl Pts',(-26.6975990820527,24.2439863218971,-61.48536084801));
#12477=CARTESIAN_POINT('Ctrl Pts',(-26.6908591135464,24.2738873474472,-61.4873040379773));
#12478=CARTESIAN_POINT('Ctrl Pts',(-26.6827770579011,24.3074995290566,-61.4894690586628));
#12479=CARTESIAN_POINT('Ctrl Pts',(-26.6818538544304,24.3113084285396,-61.4897141151567));
#12480=CARTESIAN_POINT('Ctrl Pts',(-26.6803403124962,24.3175035266299,-61.490112225576));
#12481=CARTESIAN_POINT('Ctrl Pts',(-26.6797541915127,24.3198907363365,-61.4902655194065));
#12482=CARTESIAN_POINT('Ctrl Pts',(-26.6786147521033,24.324508731492,-61.490561839627));
#12483=CARTESIAN_POINT('Ctrl Pts',(-26.6780617776622,24.3267395991493,-61.4907048857696));
#12484=CARTESIAN_POINT('Ctrl Pts',(-26.6770557404356,24.330779747765,-61.4909637605727));
#12485=CARTESIAN_POINT('Ctrl Pts',(-26.6766034948985,24.332589221457,-61.4910796362591));
#12486=CARTESIAN_POINT('Ctrl Pts',(-26.675622276029,24.336500725313,-61.4913299765845));
#12487=CARTESIAN_POINT('Ctrl Pts',(-26.6750927542741,24.3386026088715,-61.491464408499));
#12488=CARTESIAN_POINT('Ctrl Pts',(-26.673647569437,24.3443147920615,-61.4918295043768));
#12489=CARTESIAN_POINT('Ctrl Pts',(-26.6727277639275,24.3479240552917,-61.4920599275194));
#12490=CARTESIAN_POINT('Ctrl Pts',(-26.6683319939941,24.3650486878445,-61.4931519826593));
#12491=CARTESIAN_POINT('Ctrl Pts',(-26.6647744556575,24.3785432482421,-61.4940089398389));
#12492=CARTESIAN_POINT('Ctrl Pts',(-26.5989996544595,24.621625370625,-61.5093875114664));
#12493=CARTESIAN_POINT('Ctrl Pts',(-26.5116285132461,24.8436938859164,-61.5225323337839));
#12494=CARTESIAN_POINT('Ctrl Pts',(-26.3803330152951,25.0925385503838,-61.5382579594058));
#12495=CARTESIAN_POINT('Ctrl Pts',(-26.3593038722681,25.1305158703282,-61.5406861603776));
#12496=CARTESIAN_POINT('Ctrl Pts',(-26.3163995347653,25.2044343521008,-61.5454856595986));
#12497=CARTESIAN_POINT('Ctrl Pts',(-26.2945750183057,25.2403947514648,-61.5478559106757));
#12498=CARTESIAN_POINT('Ctrl Pts',(-26.2080421625401,25.3768785073722,-61.5570165434566));
#12499=CARTESIAN_POINT('Ctrl Pts',(-26.1384688842081,25.474191248581,-61.5639027718199));
#12500=CARTESIAN_POINT('Ctrl Pts',(-26.0287888974808,25.6108539554439,-61.5742939569102));
#12501=CARTESIAN_POINT('Ctrl Pts',(-25.9928029353075,25.6533853594035,-61.5776384292615));
#12502=CARTESIAN_POINT('Ctrl Pts',(-25.9509507385277,25.7003263335434,-61.5814661368066));
#12503=CARTESIAN_POINT('Ctrl Pts',(-25.9461491102277,25.7056756496338,-61.5819043915142));
#12504=CARTESIAN_POINT('Ctrl Pts',(-25.9383245841433,25.7143342130285,-61.5826171325561));
#12505=CARTESIAN_POINT('Ctrl Pts',(-25.9353125907253,25.717653317352,-61.5828911581616));
#12506=CARTESIAN_POINT('Ctrl Pts',(-25.929474526241,25.7240597405792,-61.583421646853));
#12507=CARTESIAN_POINT('Ctrl Pts',(-25.9266493439958,25.7271478601279,-61.5836780719226));
#12508=CARTESIAN_POINT('Ctrl Pts',(-25.9217655184609,25.7324653820706,-61.5841208504671));
#12509=CARTESIAN_POINT('Ctrl Pts',(-25.9197097225313,25.7346974020077,-61.5843070822777));
#12510=CARTESIAN_POINT('Ctrl Pts',(-25.9154557560405,25.7393029504051,-61.5846921332623));
#12511=CARTESIAN_POINT('Ctrl Pts',(-25.9132571585111,25.7416760785328,-61.5848909706148));
#12512=CARTESIAN_POINT('Ctrl Pts',(-25.9072964192264,25.74809059701,-61.5854295920117));
#12513=CARTESIAN_POINT('Ctrl Pts',(-25.9035274712297,25.7521256223721,-61.585769668243));
#12514=CARTESIAN_POINT('Ctrl Pts',(-25.889483711881,25.7670835876952,-61.587035048511));
#12515=CARTESIAN_POINT('Ctrl Pts',(-25.8791431926051,25.777944324224,-61.5879631882872));
#12516=CARTESIAN_POINT('Ctrl Pts',(-25.7072542936013,25.9559759004682,-61.6033345214073));
#12517=CARTESIAN_POINT('Ctrl Pts',(-25.5281944278852,26.1052214148002,-61.6186001657496));
#12518=CARTESIAN_POINT('Ctrl Pts',(-25.2633491675955,26.2813248390844,-61.6400325796174));
#12519=CARTESIAN_POINT('Ctrl Pts',(-25.1901522793135,26.3258938185981,-61.645841492262));
#12520=CARTESIAN_POINT('Ctrl Pts',(-25.0359169887877,26.4115736145694,-61.6577718219877));
#12521=CARTESIAN_POINT('Ctrl Pts',(-24.9547355244229,26.4522839216178,-61.6638861916147));
#12522=CARTESIAN_POINT('Ctrl Pts',(-24.810712171946,26.5170464231896,-61.6743425088113));
#12523=CARTESIAN_POINT('Ctrl Pts',(-24.7486337563361,26.5426609734568,-61.6787285098847));
#12524=CARTESIAN_POINT('Ctrl Pts',(-24.6679908439936,26.5730228827407,-61.6842337529714));
#12525=CARTESIAN_POINT('Ctrl Pts',(-24.6501260424632,26.5795689282214,-61.6854414164826));
#12526=CARTESIAN_POINT('Ctrl Pts',(-24.6212789724783,26.5898502746885,-61.687371183226));
#12527=CARTESIAN_POINT('Ctrl Pts',(-24.610332973953,26.5936850579361,-61.6880987600921));
#12528=CARTESIAN_POINT('Ctrl Pts',(-24.5970063191923,26.5982732502294,-61.6889787053505));
#12529=CARTESIAN_POINT('Ctrl Pts',(-24.5946453708702,26.5990830271202,-61.6891343729312));
#12530=CARTESIAN_POINT('Ctrl Pts',(-24.5900828102896,26.6006420088858,-61.6894347676971));
#12531=CARTESIAN_POINT('Ctrl Pts',(-24.5878813242596,26.601391574702,-61.6895795162321));
#12532=CARTESIAN_POINT('Ctrl Pts',(-24.5839110595067,26.6027385833994,-61.6898402082445));
#12533=CARTESIAN_POINT('Ctrl Pts',(-24.5821425772303,26.6033368708432,-61.6899562019728));
#12534=CARTESIAN_POINT('Ctrl Pts',(-24.5783392186607,26.6046198861698,-61.6902053891845));
#12535=CARTESIAN_POINT('Ctrl Pts',(-24.576304183376,26.6053041155712,-61.6903385524866));
#12536=CARTESIAN_POINT('Ctrl Pts',(-24.5708205335342,26.6071417575838,-61.6906969300287));
#12537=CARTESIAN_POINT('Ctrl Pts',(-24.5673706350273,26.6082913721803,-61.690921918089));
#12538=CARTESIAN_POINT('Ctrl Pts',(-24.5514863244174,26.6135546700965,-61.6919556693956));
#12539=CARTESIAN_POINT('Ctrl Pts',(-24.5390286233749,26.6175984452129,-61.6927603383686));
#12540=CARTESIAN_POINT('Ctrl Pts',(-24.3115467563891,26.6899092428435,-61.7073492035655));
#12541=CARTESIAN_POINT('Ctrl Pts',(-24.0899260394759,26.7354998713756,-61.7198867217408));
#12542=CARTESIAN_POINT('Ctrl Pts',(-23.7071500151676,26.7731026460078,-61.7413772570515));
#12543=CARTESIAN_POINT('Ctrl Pts',(-23.548044804176,26.776918044297,-61.7502606007284));
#12544=CARTESIAN_POINT('Ctrl Pts',(-23.286282235583,26.7638299552651,-61.7654177473956));
#12545=CARTESIAN_POINT('Ctrl Pts',(-23.1835640776844,26.7537344582914,-61.7715012318966));
#12546=CARTESIAN_POINT('Ctrl Pts',(-23.0622730692102,26.7359034568069,-61.7789206071396));
#12547=CARTESIAN_POINT('Ctrl Pts',(-23.0430585881178,26.7329008079353,-61.7801029610204));
#12548=CARTESIAN_POINT('Ctrl Pts',(-23.0195516456687,26.7290090992961,-61.7815583839449));
#12549=CARTESIAN_POINT('Ctrl Pts',(-23.0152319891155,26.7282849049121,-61.7818262040267));
#12550=CARTESIAN_POINT('Ctrl Pts',(-23.0068600927136,26.7268637962524,-61.7823459879673));
#12551=CARTESIAN_POINT('Ctrl Pts',(-23.0028076819765,26.7261679280999,-61.7825979181069));
#12552=CARTESIAN_POINT('Ctrl Pts',(-22.9957760806056,26.7249466239421,-61.7830356338216));
#12553=CARTESIAN_POINT('Ctrl Pts',(-22.9927962707597,26.7244247436591,-61.783221305852));
#12554=CARTESIAN_POINT('Ctrl Pts',(-22.9865995584043,26.7233304639753,-61.7836077984385));
#12555=CARTESIAN_POINT('Ctrl Pts',(-22.9833827840009,26.7227573666228,-61.783808641068));
#12556=CARTESIAN_POINT('Ctrl Pts',(-22.9755369615362,26.7213472487683,-61.784299019455));
#12557=CARTESIAN_POINT('Ctrl Pts',(-22.9709088736536,26.720504984853,-61.7845887223181));
#12558=CARTESIAN_POINT('Ctrl Pts',(-22.9533455239478,26.7172688938658,-61.7856898077358));
#12559=CARTESIAN_POINT('Ctrl Pts',(-22.9404232558358,26.7148060326194,-61.7865033926721));
#12560=CARTESIAN_POINT('Ctrl Pts',(-22.7157639893085,26.6705609700712,-61.8007092585757));
#12561=CARTESIAN_POINT('Ctrl Pts',(-22.5087797959071,26.6077019281494,-61.8148044895628));
#12562=CARTESIAN_POINT('Ctrl Pts',(-22.229998003443,26.491425106261,-61.835092358332));
#12563=CARTESIAN_POINT('Ctrl Pts',(-22.1517269529096,26.4550217759146,-61.8409354953986));
#12564=CARTESIAN_POINT('Ctrl Pts',(-22.0750358661665,26.4155366977499,-61.8467738923868));
#12565=CARTESIAN_POINT('',(-26.7730032083997,23.5493289177337,-61.6829767636861));
#12566=CARTESIAN_POINT('Ctrl Pts',(-22.0750361387181,26.4155368380754,-62.0907209741597));
#12567=CARTESIAN_POINT('Ctrl Pts',(-22.1348983042596,26.4463573914597,-62.0862507094239));
#12568=CARTESIAN_POINT('Ctrl Pts',(-22.1957343443035,26.4753060929015,-62.0818347705942));
#12569=CARTESIAN_POINT('Ctrl Pts',(-22.2890802308409,26.5161847309523,-62.0752946354846));
#12570=CARTESIAN_POINT('Ctrl Pts',(-22.3209256529958,26.5295251020064,-62.0731038077036));
#12571=CARTESIAN_POINT('Ctrl Pts',(-22.3572481549109,26.5440593466051,-62.0706554199582));
#12572=CARTESIAN_POINT('Ctrl Pts',(-22.3615191346708,26.5457577644479,-62.0703683104026));
#12573=CARTESIAN_POINT('Ctrl Pts',(-22.3679934679548,26.5483163507416,-62.0699342866162));
#12574=CARTESIAN_POINT('Ctrl Pts',(-22.3701941362364,26.5491832311724,-62.0697869691642));
#12575=CARTESIAN_POINT('Ctrl Pts',(-22.3740254197869,26.5506875683066,-62.0695308627783));
#12576=CARTESIAN_POINT('Ctrl Pts',(-22.3756555999684,26.5513261188846,-62.0694220073787));
#12577=CARTESIAN_POINT('Ctrl Pts',(-22.3790362690513,26.5526471690822,-62.0691965041688));
#12578=CARTESIAN_POINT('Ctrl Pts',(-22.3807868334832,26.5533294659775,-62.0690798690874));
#12579=CARTESIAN_POINT('Ctrl Pts',(-22.3849564955543,26.5549504272834,-62.068802373458));
#12580=CARTESIAN_POINT('Ctrl Pts',(-22.3873761391432,26.5558877043928,-62.0686415973042));
#12581=CARTESIAN_POINT('Ctrl Pts',(-22.3925163477922,26.5578716877665,-62.068300583244));
#12582=CARTESIAN_POINT('Ctrl Pts',(-22.3952372087995,26.5589176282987,-62.0681203914689));
#12583=CARTESIAN_POINT('Ctrl Pts',(-22.4026515583563,26.5617562774942,-62.0676302214017));
#12584=CARTESIAN_POINT('Ctrl Pts',(-22.4073478501987,26.5635417137648,-62.0673206744759));
#12585=CARTESIAN_POINT('Ctrl Pts',(-22.4220208515739,26.5690808577836,-62.066356374561));
#12586=CARTESIAN_POINT('Ctrl Pts',(-22.4320121442184,26.5727961011927,-62.065703848325));
#12587=CARTESIAN_POINT('Ctrl Pts',(-22.4698076656402,26.5866372316084,-62.0632502172207));
#12588=CARTESIAN_POINT('Ctrl Pts',(-22.4977334142995,26.5964299396005,-62.0614674125305));
#12589=CARTESIAN_POINT('Ctrl Pts',(-22.5893792252394,26.6271564972446,-62.0557023313666));
#12590=CARTESIAN_POINT('Ctrl Pts',(-22.6536215535954,26.6464872752498,-62.0517950470289));
#12591=CARTESIAN_POINT('Ctrl Pts',(-23.0927241919434,26.7637997439734,-62.0256999094175));
#12592=CARTESIAN_POINT('Ctrl Pts',(-23.4819674535229,26.7954937877334,-62.0051092222063));
#12593=CARTESIAN_POINT('Ctrl Pts',(-23.8874729132588,26.7553735015161,-61.9804611769144));
#12594=CARTESIAN_POINT('Ctrl Pts',(-23.9073678962075,26.7532178148759,-61.9792450238951));
#12595=CARTESIAN_POINT('Ctrl Pts',(-23.9334066288751,26.7501508176658,-61.9776439057701));
#12596=CARTESIAN_POINT('Ctrl Pts',(-23.9395699416906,26.7494068037124,-61.9772642331572));
#12597=CARTESIAN_POINT('Ctrl Pts',(-23.949078356347,26.7482310963465,-61.976677415551));
#12598=CARTESIAN_POINT('Ctrl Pts',(-23.9524250183405,26.7478119493177,-61.9764706676532));
#12599=CARTESIAN_POINT('Ctrl Pts',(-23.959088216047,26.7469668020992,-61.9760586189606));
#12600=CARTESIAN_POINT('Ctrl Pts',(-23.9624047591763,26.7465408923805,-61.9758533212689));
#12601=CARTESIAN_POINT('Ctrl Pts',(-23.9697553688048,26.7455852978474,-61.9753978546151));
#12602=CARTESIAN_POINT('Ctrl Pts',(-23.973789102262,26.7450531342272,-61.9751476074535));
#12603=CARTESIAN_POINT('Ctrl Pts',(-23.9854247810781,26.7434956350085,-61.9744248616323));
#12604=CARTESIAN_POINT('Ctrl Pts',(-23.9930240487318,26.7424508002183,-61.9739517458308));
#12605=CARTESIAN_POINT('Ctrl Pts',(-24.0442403191113,26.7352225954622,-61.9707556781446));
#12606=CARTESIAN_POINT('Ctrl Pts',(-24.0877285039204,26.7281728437512,-61.968005356302));
#12607=CARTESIAN_POINT('Ctrl Pts',(-24.1979051597372,26.7079862670966,-61.960939936521));
#12608=CARTESIAN_POINT('Ctrl Pts',(-24.2643449674852,26.6936276546812,-61.9565873208804));
#12609=CARTESIAN_POINT('Ctrl Pts',(-24.5019507564445,26.6343559187636,-61.9406852691831));
#12610=CARTESIAN_POINT('Ctrl Pts',(-24.6697871274292,26.5774710992069,-61.9287942516228));
#12611=CARTESIAN_POINT('Ctrl Pts',(-24.9054751209075,26.4752973085792,-61.9114091623848));
#12612=CARTESIAN_POINT('Ctrl Pts',(-24.977652389534,26.4407620354602,-61.9059893068155));
#12613=CARTESIAN_POINT('Ctrl Pts',(-25.1734897905367,26.3379320953801,-61.8911182266855));
#12614=CARTESIAN_POINT('Ctrl Pts',(-25.2940771427177,26.2641322271398,-61.8817676627819));
#12615=CARTESIAN_POINT('Ctrl Pts',(-25.4160790971411,26.1779653607126,-61.8723865830397));
#12616=CARTESIAN_POINT('Ctrl Pts',(-25.4226933688041,26.1732563058107,-61.8718782696924));
#12617=CARTESIAN_POINT('Ctrl Pts',(-25.4315118798352,26.1669275798934,-61.8712010076892));
#12618=CARTESIAN_POINT('Ctrl Pts',(-25.4337318806904,26.1653300802335,-61.8710305497779));
#12619=CARTESIAN_POINT('Ctrl Pts',(-25.4374508910095,26.1626467096814,-61.8707450616491));
#12620=CARTESIAN_POINT('Ctrl Pts',(-25.4389509981492,26.1615623737918,-61.870629925186));
#12621=CARTESIAN_POINT('Ctrl Pts',(-25.4419408429953,26.1593972733161,-61.8704004865963));
#12622=CARTESIAN_POINT('Ctrl Pts',(-25.4434305791984,26.1583165321198,-61.8702861846003));
#12623=CARTESIAN_POINT('Ctrl Pts',(-25.4467797092904,26.155882496946,-61.8700292606121));
#12624=CARTESIAN_POINT('Ctrl Pts',(-25.4486385772807,26.1545284911848,-61.8698866893688));
#12625=CARTESIAN_POINT('Ctrl Pts',(-25.4538913606107,26.1506937335384,-61.8694838899747));
#12626=CARTESIAN_POINT('Ctrl Pts',(-25.4572818894172,26.1482083173969,-61.8692239861287));
#12627=CARTESIAN_POINT('Ctrl Pts',(-25.4650639723633,26.1424802434008,-61.8686276316466));
#12628=CARTESIAN_POINT('Ctrl Pts',(-25.4694521848803,26.1392330366195,-61.8682914931845));
#12629=CARTESIAN_POINT('Ctrl Pts',(-25.4834040274463,26.128853932152,-61.8672231429246));
#12630=CARTESIAN_POINT('Ctrl Pts',(-25.4929364489092,26.1216799749388,-61.8664937546918));
#12631=CARTESIAN_POINT('Ctrl Pts',(-25.5298875130364,26.0935484015138,-61.8636675782526));
#12632=CARTESIAN_POINT('Ctrl Pts',(-25.5570097274758,26.0722030291371,-61.8615957246152));
#12633=CARTESIAN_POINT('Ctrl Pts',(-25.6626739232377,25.9862603336209,-61.8535110758957));
#12634=CARTESIAN_POINT('Ctrl Pts',(-25.7384885022577,25.918392077268,-61.8476804035136));
#12635=CARTESIAN_POINT('Ctrl Pts',(-26.0565060257945,25.6053695221999,-61.8224506829145));
#12636=CARTESIAN_POINT('Ctrl Pts',(-26.261677137006,25.3259170459436,-61.8037785449454));
#12637=CARTESIAN_POINT('Ctrl Pts',(-26.4281728551776,25.0008119090734,-61.7816941450935));
#12638=CARTESIAN_POINT('Ctrl Pts',(-26.4374501167941,24.9822574091092,-61.7804337653922));
#12639=CARTESIAN_POINT('Ctrl Pts',(-26.4493087636323,24.9579563964744,-61.778782622177));
#12640=CARTESIAN_POINT('Ctrl Pts',(-26.4520534846625,24.9522897763206,-61.7783975725911));
#12641=CARTESIAN_POINT('Ctrl Pts',(-26.456250659572,24.943559367785,-61.7778042801224));
#12642=CARTESIAN_POINT('Ctrl Pts',(-26.4577149246208,24.9405012476816,-61.777596448705));
#12643=CARTESIAN_POINT('Ctrl Pts',(-26.460599339484,24.9344526547493,-61.7771853595334));
#12644=CARTESIAN_POINT('Ctrl Pts',(-26.4620197130027,24.931462292738,-61.7769821098694));
#12645=CARTESIAN_POINT('Ctrl Pts',(-26.4651573198628,24.9248302302335,-61.7765313123871));
#12646=CARTESIAN_POINT('Ctrl Pts',(-26.4668723393945,24.9211874938662,-61.7762836881453));
#12647=CARTESIAN_POINT('Ctrl Pts',(-26.4717508164815,24.9107749213434,-61.775575808498));
#12648=CARTESIAN_POINT('Ctrl Pts',(-26.4748975454269,24.9039973166864,-61.77511497477));
#12649=CARTESIAN_POINT('Ctrl Pts',(-26.4947749712628,24.8607913924581,-61.7721767232056));
#12650=CARTESIAN_POINT('Ctrl Pts',(-26.5108477102306,24.8240658843355,-61.7696767393512));
#12651=CARTESIAN_POINT('Ctrl Pts',(-26.5565740976545,24.7140393225136,-61.7621757810922));
#12652=CARTESIAN_POINT('Ctrl Pts',(-26.5842180297521,24.6399408726663,-61.7571088459108));
#12653=CARTESIAN_POINT('Ctrl Pts',(-26.7177887014048,24.237267997524,-61.7294873244182));
#12654=CARTESIAN_POINT('Ctrl Pts',(-26.7731008870704,23.8943916030023,-61.7053486917779));
#12655=CARTESIAN_POINT('Ctrl Pts',(-26.7730024004244,23.5493326950576,-61.6829756068469));
#12656=CARTESIAN_POINT('Ctrl Pts',(-26.7730023993701,23.5493290084874,-61.6829753678154));
#12657=CARTESIAN_POINT('Ctrl Pts',(-26.77298796788,23.4989685168407,-61.6797100738703));
#12658=CARTESIAN_POINT('Ctrl Pts',(-26.7717930925859,23.4486111574792,-61.6764920584389));
#12659=CARTESIAN_POINT('Ctrl Pts',(-26.7692328724598,23.3943725239603,-61.6730914108621));
#12660=CARTESIAN_POINT('Ctrl Pts',(-26.7690403661588,23.3904467491426,-61.6728456432062));
#12661=CARTESIAN_POINT('Ctrl Pts',(-26.7687155509059,23.3840616106022,-61.6724465234169));
#12662=CARTESIAN_POINT('Ctrl Pts',(-26.7685876045742,23.3816020438382,-61.6722929297187));
#12663=CARTESIAN_POINT('Ctrl Pts',(-26.7683579156123,23.3772820954303,-61.6720234226909));
#12664=CARTESIAN_POINT('Ctrl Pts',(-26.768257379174,23.375421654951,-61.6719074416966));
#12665=CARTESIAN_POINT('Ctrl Pts',(-26.7680577452648,23.3717859200148,-61.6716809564883));
#12666=CARTESIAN_POINT('Ctrl Pts',(-26.7679587917668,23.3700106167124,-61.6715704440393));
#12667=CARTESIAN_POINT('Ctrl Pts',(-26.7677588472377,23.3664760997634,-61.6713505784151));
#12668=CARTESIAN_POINT('Ctrl Pts',(-26.7676578827629,23.3647168897093,-61.6712412239035));
#12669=CARTESIAN_POINT('Ctrl Pts',(-26.7674154396115,23.3605522616753,-61.6709825278229));
#12670=CARTESIAN_POINT('Ctrl Pts',(-26.7672727057288,23.3581469136953,-61.6708332574662));
#12671=CARTESIAN_POINT('Ctrl Pts',(-26.7668394262751,23.3509812157547,-61.6703889929946));
#12672=CARTESIAN_POINT('Ctrl Pts',(-26.7665410096811,23.3462213213228,-61.6700944406322));
#12673=CARTESIAN_POINT('Ctrl Pts',(-26.7636913419284,23.3023281615626,-61.667383216405));
#12674=CARTESIAN_POINT('Ctrl Pts',(-26.7604364223237,23.2632417158167,-61.6650053901776));
#12675=CARTESIAN_POINT('Ctrl Pts',(-26.7559160695493,23.2187880830934,-61.6623328016616));
#12676=CARTESIAN_POINT('Ctrl Pts',(-26.7553496617834,23.2133552385687,-61.6620067162069));
#12677=CARTESIAN_POINT('Ctrl Pts',(-26.7535324870158,23.1963447830095,-61.6609873530432));
#12678=CARTESIAN_POINT('Ctrl Pts',(-26.7522327671734,23.1847723740444,-61.6602962251322));
#12679=CARTESIAN_POINT('Ctrl Pts',(-26.71680429906,22.8840314575788,-61.6423908248603));
#12680=CARTESIAN_POINT('Ctrl Pts',(-26.6437033804265,22.6007760681689,-61.626752536299));
#12681=CARTESIAN_POINT('Ctrl Pts',(-26.4952981481866,22.2376065449688,-61.6044334485409));
#12682=CARTESIAN_POINT('Ctrl Pts',(-26.4526877085093,22.1459019181378,-61.598597310402));
#12683=CARTESIAN_POINT('Ctrl Pts',(-26.3758231662176,21.998975049912,-61.5887906099315));
#12684=CARTESIAN_POINT('Ctrl Pts',(-26.3440835948615,21.9425155127872,-61.5849058753863));
#12685=CARTESIAN_POINT('Ctrl Pts',(-26.3063146808832,21.8798303995179,-61.580444959906));
#12686=CARTESIAN_POINT('Ctrl Pts',(-26.3019345219486,21.8726247743425,-61.5799299292277));
#12687=CARTESIAN_POINT('Ctrl Pts',(-26.2953160648788,21.861832668847,-61.57915513239));
#12688=CARTESIAN_POINT('Ctrl Pts',(-26.293098883079,21.8582332271638,-61.5788961443316));
#12689=CARTESIAN_POINT('Ctrl Pts',(-26.2892748873779,21.8520525015314,-61.5784504353641));
#12690=CARTESIAN_POINT('Ctrl Pts',(-26.2876714870989,21.8494691034275,-61.5782638407588));
#12691=CARTESIAN_POINT('Ctrl Pts',(-26.2843631703712,21.8441555419157,-61.5778794335847));
#12692=CARTESIAN_POINT('Ctrl Pts',(-26.2826578152181,21.8414256564661,-61.5776816048979));
#12693=CARTESIAN_POINT('Ctrl Pts',(-26.2785446123238,21.8348632548158,-61.5772052297454));
#12694=CARTESIAN_POINT('Ctrl Pts',(-26.2761327796085,21.8310332547661,-61.5769265355586));
#12695=CARTESIAN_POINT('Ctrl Pts',(-26.2687131782411,21.8193057607094,-61.5760711109888));
#12696=CARTESIAN_POINT('Ctrl Pts',(-26.2636791307752,21.811425024652,-61.5754934031743));
#12697=CARTESIAN_POINT('Ctrl Pts',(-26.2050136701497,21.7204601477895,-61.568791499522));
#12698=CARTESIAN_POINT('Ctrl Pts',(-26.1476251094473,21.6398732243153,-61.5625261077611));
#12699=CARTESIAN_POINT('Ctrl Pts',(-25.9066228427523,21.3324222915602,-61.537247804175));
#12700=CARTESIAN_POINT('Ctrl Pts',(-25.696275748339,21.1283140911703,-61.5171696679778));
#12701=CARTESIAN_POINT('Ctrl Pts',(-25.4259614124385,20.929227555305,-61.494745387239));
#12702=CARTESIAN_POINT('Ctrl Pts',(-25.3899807431336,20.9038481553379,-61.4918242623714));
#12703=CARTESIAN_POINT('Ctrl Pts',(-25.3101847814587,20.8499773384049,-61.4855007852995));
#12704=CARTESIAN_POINT('Ctrl Pts',(-25.2661720418521,20.8217971875919,-61.482111285724));
#12705=CARTESIAN_POINT('Ctrl Pts',(-25.207362350812,20.7861292257318,-61.4777289163152));
#12706=CARTESIAN_POINT('Ctrl Pts',(-25.1931678102999,20.7776688959699,-61.4766821540836));
#12707=CARTESIAN_POINT('Ctrl Pts',(-25.1729172289965,20.76580913142,-61.4752050126637));
#12708=CARTESIAN_POINT('Ctrl Pts',(-25.1669145846239,20.7623196813717,-61.4747691677191));
#12709=CARTESIAN_POINT('Ctrl Pts',(-25.1577199487639,20.7570143480418,-61.4741046744202));
#12710=CARTESIAN_POINT('Ctrl Pts',(-25.1545360988026,20.7551845031523,-61.4738751481009));
#12711=CARTESIAN_POINT('Ctrl Pts',(-25.1486373277577,20.7518077189741,-61.4734509639567));
#12712=CARTESIAN_POINT('Ctrl Pts',(-25.1459232759393,20.7502592812942,-61.4732562102904));
#12713=CARTESIAN_POINT('Ctrl Pts',(-25.141472707935,20.7477286882182,-61.4729375340816));
#12714=CARTESIAN_POINT('Ctrl Pts',(-25.139737532262,20.7467441982753,-61.4728134598668));
#12715=CARTESIAN_POINT('Ctrl Pts',(-25.1363909274929,20.7448495344469,-61.4725744899994));
#12716=CARTESIAN_POINT('Ctrl Pts',(-25.1347796327376,20.7439391397753,-61.4724595802872));
#12717=CARTESIAN_POINT('Ctrl Pts',(-25.1310236056667,20.7418212200615,-61.4721920603812));
#12718=CARTESIAN_POINT('Ctrl Pts',(-25.1288782677416,20.7406147603697,-61.4720395196366));
#12719=CARTESIAN_POINT('Ctrl Pts',(-25.1231381391869,20.7373953716967,-61.4716320639902));
#12720=CARTESIAN_POINT('Ctrl Pts',(-25.1195408520804,20.7353868679806,-61.4713774344176));
#12721=CARTESIAN_POINT('Ctrl Pts',(-25.0947394809378,20.7216016290153,-61.4696267784791));
#12722=CARTESIAN_POINT('Ctrl Pts',(-25.0734061478839,20.7100572898994,-61.4681454461586));
#12723=CARTESIAN_POINT('Ctrl Pts',(-24.8958300525273,20.6165399666368,-61.455999695206));
#12724=CARTESIAN_POINT('Ctrl Pts',(-24.7332052316643,20.5472725859317,-61.4460416360131));
#12725=CARTESIAN_POINT('Ctrl Pts',(-24.5492041631577,20.4861840659201,-61.4351857125989));
#12726=CARTESIAN_POINT('Ctrl Pts',(-24.5326572158684,20.4808387498048,-61.4342130889292));
#12727=CARTESIAN_POINT('Ctrl Pts',(-24.4972920077689,20.4697296688511,-61.4321407115824));
#12728=CARTESIAN_POINT('Ctrl Pts',(-24.4784625870231,20.4640038423793,-61.4310411415158));
#12729=CARTESIAN_POINT('Ctrl Pts',(-24.4378898825118,20.4520710100127,-61.4286781246671));
#12730=CARTESIAN_POINT('Ctrl Pts',(-24.4161313664937,20.445919648689,-61.4274147222222));
#12731=CARTESIAN_POINT('Ctrl Pts',(-24.3687391414372,20.4330584001663,-61.4246684341453));
#12732=CARTESIAN_POINT('Ctrl Pts',(-24.3430838444238,20.4264346624111,-61.4231852416972));
#12733=CARTESIAN_POINT('Ctrl Pts',(-24.286274395182,20.4125124110083,-61.4199042787008));
#12734=CARTESIAN_POINT('Ctrl Pts',(-24.2550874997141,20.405360025295,-61.4181052970364));
#12735=CARTESIAN_POINT('Ctrl Pts',(-24.0456409529083,20.360597672067,-61.4060166067711));
#12736=CARTESIAN_POINT('Ctrl Pts',(-23.8646011426449,20.3377023925571,-61.3955076210613));
#12737=CARTESIAN_POINT('Ctrl Pts',(-23.6646136032446,20.3294818770431,-61.383383536608));
#12738=CARTESIAN_POINT('Ctrl Pts',(-23.6466092679616,20.3288929703637,-61.3822877408049));
#12739=CARTESIAN_POINT('Ctrl Pts',(-23.622876154311,20.3283158209997,-61.3808373233665));
#12740=CARTESIAN_POINT('Ctrl Pts',(-23.6171507551954,20.3281918579474,-61.380486967183));
#12741=CARTESIAN_POINT('Ctrl Pts',(-23.6077857516741,20.3280140643208,-61.3799131351714));
#12742=CARTESIAN_POINT('Ctrl Pts',(-23.6041463156831,20.3279511379856,-61.3796899452571));
#12743=CARTESIAN_POINT('Ctrl Pts',(-23.5971190791077,20.3278415447733,-61.3792586333764));
#12744=CARTESIAN_POINT('Ctrl Pts',(-23.5937312946503,20.3277940542384,-61.3790505375629));
#12745=CARTESIAN_POINT('Ctrl Pts',(-23.5859454374688,20.3276971908968,-61.3785719107915));
#12746=CARTESIAN_POINT('Ctrl Pts',(-23.5815473331898,20.3276514792651,-61.3783012652277));
#12747=CARTESIAN_POINT('Ctrl Pts',(-23.5676092977153,20.3275351502584,-61.3774426760297));
#12748=CARTESIAN_POINT('Ctrl Pts',(-23.5580692059021,20.3274978909561,-61.3768536863905));
#12749=CARTESIAN_POINT('Ctrl Pts',(-23.4768855723816,20.3275413037916,-61.3718301398985));
#12750=CARTESIAN_POINT('Ctrl Pts',(-23.4052682892536,20.3299685987673,-61.3673222932025));
#12751=CARTESIAN_POINT('Ctrl Pts',(-23.2758893200614,20.3386780366423,-61.359030749554));
#12752=CARTESIAN_POINT('Ctrl Pts',(-23.218101812269,20.3441394404512,-61.3552736995221));
#12753=CARTESIAN_POINT('Ctrl Pts',(-23.1570944813177,20.3515721707212,-61.3512516503649));
#12754=CARTESIAN_POINT('Ctrl Pts',(-23.1536936813346,20.3519920072328,-61.351027261994));
#12755=CARTESIAN_POINT('Ctrl Pts',(-22.8910522854692,20.3848410354703,-61.3336838329514));
#12756=CARTESIAN_POINT('Ctrl Pts',(-22.6367259409956,20.4486696273512,-61.3157162825649));
#12757=CARTESIAN_POINT('Ctrl Pts',(-22.3521784229073,20.5581556764268,-61.2953673878405));
#12758=CARTESIAN_POINT('Ctrl Pts',(-22.3117371990433,20.5746676791203,-61.2924721076232));
#12759=CARTESIAN_POINT('Ctrl Pts',(-22.2249782366115,20.6121664242863,-61.2862709184932));
#12760=CARTESIAN_POINT('Ctrl Pts',(-22.1787945632529,20.6334382401077,-61.2829762510978));
#12761=CARTESIAN_POINT('Ctrl Pts',(-22.118747894696,20.662836993012,-61.2787188723746));
#12762=CARTESIAN_POINT('Ctrl Pts',(-22.104417314616,20.6699861259441,-61.2777048283309));
#12763=CARTESIAN_POINT('Ctrl Pts',(-22.0840922002756,20.6803156905262,-61.2762701084281));
#12764=CARTESIAN_POINT('Ctrl Pts',(-22.0780537708292,20.683408552651,-61.2758443078438));
#12765=CARTESIAN_POINT('Ctrl Pts',(-22.0688161183545,20.6881769287432,-61.2751936460567));
#12766=CARTESIAN_POINT('Ctrl Pts',(-22.0656099151044,20.6898387670295,-61.2749679500923));
#12767=CARTESIAN_POINT('Ctrl Pts',(-22.0603405970504,20.6925812046347,-61.2745972559877));
#12768=CARTESIAN_POINT('Ctrl Pts',(-22.0582758588014,20.6936586518928,-61.2744520612587));
#12769=CARTESIAN_POINT('Ctrl Pts',(-22.0543641604898,20.6957053007023,-61.27417710009));
#12770=CARTESIAN_POINT('Ctrl Pts',(-22.0525169714267,20.6966740581567,-61.2740473056566));
#12771=CARTESIAN_POINT('Ctrl Pts',(-22.0490532601842,20.6984948896671,-61.2738040171793));
#12772=CARTESIAN_POINT('Ctrl Pts',(-22.0474365282364,20.6993465421115,-61.2736904971235));
#12773=CARTESIAN_POINT('Ctrl Pts',(-22.0441402472675,20.701086520535,-61.273459123774));
#12774=CARTESIAN_POINT('Ctrl Pts',(-22.0424607658326,20.701974953351,-61.273341278081));
#12775=CARTESIAN_POINT('Ctrl Pts',(-22.0376292608331,20.7045362533843,-61.2730023763507));
#12776=CARTESIAN_POINT('Ctrl Pts',(-22.0344792160151,20.7062128779698,-61.2727815600118));
#12777=CARTESIAN_POINT('Ctrl Pts',(-22.0206665207952,20.7135942101874,-61.2718138878588));
#12778=CARTESIAN_POINT('Ctrl Pts',(-22.0100330617969,20.7193537710198,-61.2710704874358));
#12779=CARTESIAN_POINT('Ctrl Pts',(-21.9963574789405,20.7268609489837,-61.2701160780696));
#12780=CARTESIAN_POINT('Ctrl Pts',(-21.9932856230027,20.7285537685751,-61.2699018046384));
#12781=CARTESIAN_POINT('Ctrl Pts',(-21.7507628691689,20.862718345016,-61.2529930856901));
#12782=CARTESIAN_POINT('Ctrl Pts',(-21.5291113834145,21.0251690425092,-61.2381040094146));
#12783=CARTESIAN_POINT('Ctrl Pts',(-21.3046575496665,21.2383907919833,-61.2207371433525));
#12784=CARTESIAN_POINT('Ctrl Pts',(-21.2790922029574,21.2635010736892,-61.2187216805558));
#12785=CARTESIAN_POINT('Ctrl Pts',(-21.2235379498319,21.3199172053114,-61.2142481800868));
#12786=CARTESIAN_POINT('Ctrl Pts',(-21.1937515672006,21.3514120494542,-61.2117864113642));
#12787=CARTESIAN_POINT('Ctrl Pts',(-21.0964333316423,21.4585614529659,-61.203504096158));
#12788=CARTESIAN_POINT('Ctrl Pts',(-21.0318428471099,21.5367952855778,-61.197604202909));
#12789=CARTESIAN_POINT('Ctrl Pts',(-20.9426911398844,21.6557926162066,-61.1887364618861));
#12790=CARTESIAN_POINT('Ctrl Pts',(-20.9151692044089,21.6942648482234,-61.1858851418246));
#12791=CARTESIAN_POINT('Ctrl Pts',(-20.8840975042437,21.7397840710182,-61.1825241248383));
#12792=CARTESIAN_POINT('Ctrl Pts',(-20.8797136244607,21.746256794239,-61.1820464903697));
#12793=CARTESIAN_POINT('Ctrl Pts',(-20.8730666668809,21.7561482380885,-61.1813170037548));
#12794=CARTESIAN_POINT('Ctrl Pts',(-20.8707864683667,21.7595554645383,-61.1810657992602));
#12795=CARTESIAN_POINT('Ctrl Pts',(-20.8666574289854,21.7657508983119,-61.1806091622433));
#12796=CARTESIAN_POINT('Ctrl Pts',(-20.8648064135042,21.7685376552369,-61.180403812082));
#12797=CARTESIAN_POINT('Ctrl Pts',(-20.861108115814,21.7741244041445,-61.179992231971));
#12798=CARTESIAN_POINT('Ctrl Pts',(-20.8592608592962,21.7769244081134,-61.1797860013945));
#12799=CARTESIAN_POINT('Ctrl Pts',(-20.8540573776195,21.7848385088804,-61.1792032305848));
#12800=CARTESIAN_POINT('Ctrl Pts',(-20.8507113498022,21.7899592642963,-61.178826308423));
#12801=CARTESIAN_POINT('Ctrl Pts',(-20.8368808354316,21.8112576378784,-61.1772592189583));
#12802=CARTESIAN_POINT('Ctrl Pts',(-20.8265272042747,21.8275193783688,-61.176064178685));
#12803=CARTESIAN_POINT('Ctrl Pts',(-20.6086486206086,22.1766006881929,-61.1504381721112));
#12804=CARTESIAN_POINT('Ctrl Pts',(-20.4634993853836,22.544408513569,-61.1233633556784));
#12805=CARTESIAN_POINT('Ctrl Pts',(-20.3731386491286,23.0043932739609,-61.0921837777148));
#12806=CARTESIAN_POINT('Ctrl Pts',(-20.3610327448102,23.0802589132278,-61.0871448907393));
#12807=CARTESIAN_POINT('Ctrl Pts',(-20.3491325452743,23.1769264523618,-61.0809121059813));
#12808=CARTESIAN_POINT('Ctrl Pts',(-20.3468125973796,23.1973868823462,-61.0796035108678));
#12809=CARTESIAN_POINT('Ctrl Pts',(-20.3438465790326,23.2259916485801,-61.07779014952));
#12810=CARTESIAN_POINT('Ctrl Pts',(-20.3430351848222,23.2341178343324,-61.0772768149464));
#12811=CARTESIAN_POINT('Ctrl Pts',(-20.3418597536872,23.2463604131877,-61.0765062664883));
#12812=CARTESIAN_POINT('Ctrl Pts',(-20.3414727380289,23.2504744906828,-61.0762478055664));
#12813=CARTESIAN_POINT('Ctrl Pts',(-20.340859945409,23.2571258049654,-61.0758307335309));
#12814=CARTESIAN_POINT('Ctrl Pts',(-20.3406292634172,23.25966256857,-61.0756718502347));
#12815=CARTESIAN_POINT('Ctrl Pts',(-20.3401988168299,23.2644591503669,-61.0753717825014));
#12816=CARTESIAN_POINT('Ctrl Pts',(-20.3399984305386,23.2667189089752,-61.0752305631692));
#12817=CARTESIAN_POINT('Ctrl Pts',(-20.3396397844556,23.270812488616,-61.0749750132988));
#12818=CARTESIAN_POINT('Ctrl Pts',(-20.3394807095987,23.272646233295,-61.074860636567));
#12819=CARTESIAN_POINT('Ctrl Pts',(-20.3391674385432,23.2762937745336,-61.0746333238387));
#12820=CARTESIAN_POINT('Ctrl Pts',(-20.339013208611,23.2781075592907,-61.0745203861826));
#12821=CARTESIAN_POINT('Ctrl Pts',(-20.3385943690745,23.2830831546975,-61.0742108363067));
#12822=CARTESIAN_POINT('Ctrl Pts',(-20.338332890962,23.2862452378341,-61.0740144017979));
#12823=CARTESIAN_POINT('Ctrl Pts',(-20.3373468077685,23.2983883706379,-61.0732611441404));
#12824=CARTESIAN_POINT('Ctrl Pts',(-20.3366551891144,23.3073721685507,-61.0727061674145));
#12825=CARTESIAN_POINT('Ctrl Pts',(-20.3255375831517,23.460154333673,-61.0633053450626));
#12826=CARTESIAN_POINT('Ctrl Pts',(-20.3247336543253,23.6045115540161,-61.0549823666806));
#12827=CARTESIAN_POINT('Ctrl Pts',(-20.3369578055946,23.8028982024527,-61.0437356743519));
#12828=CARTESIAN_POINT('Ctrl Pts',(-20.3416941626172,23.8572480287291,-61.0406748536807));
#12829=CARTESIAN_POINT('Ctrl Pts',(-20.3662416448557,24.0748892353054,-61.0284172659998));
#12830=CARTESIAN_POINT('Ctrl Pts',(-20.3971597414454,24.2366723897695,-61.0192903463121));
#12831=CARTESIAN_POINT('Ctrl Pts',(-20.4773336689076,24.5317018087349,-61.0017778432566));
#12832=CARTESIAN_POINT('Ctrl Pts',(-20.523296451582,24.6654215242556,-60.9934906497151));
#12833=CARTESIAN_POINT('Ctrl Pts',(-20.581962124228,24.8054343395217,-60.9842517399167));
#12834=CARTESIAN_POINT('Ctrl Pts',(-20.5860952919551,24.8151640573253,-60.9836067638771));
#12835=CARTESIAN_POINT('Ctrl Pts',(-20.5921102740048,24.8291322952589,-60.9826765070969));
#12836=CARTESIAN_POINT('Ctrl Pts',(-20.5939535136893,24.8333874358137,-60.9823925452525));
#12837=CARTESIAN_POINT('Ctrl Pts',(-20.5971700661699,24.8407691630625,-60.9818989240029));
#12838=CARTESIAN_POINT('Ctrl Pts',(-20.5985391798708,24.8438975805958,-60.9816894087184));
#12839=CARTESIAN_POINT('Ctrl Pts',(-20.6011824346483,24.8499113615375,-60.9812860454844));
#12840=CARTESIAN_POINT('Ctrl Pts',(-20.6024558450807,24.8527970436215,-60.9810922227939));
#12841=CARTESIAN_POINT('Ctrl Pts',(-20.6054674504959,24.8595946231108,-60.9806350083226));
#12842=CARTESIAN_POINT('Ctrl Pts',(-20.6072092043423,24.8635049293154,-60.9803714943829));
#12843=CARTESIAN_POINT('Ctrl Pts',(-20.6123812643214,24.875054442719,-60.9795916868885));
#12844=CARTESIAN_POINT('Ctrl Pts',(-20.6158335404669,24.8826837190019,-60.9790746371937));
#12845=CARTESIAN_POINT('Ctrl Pts',(-20.6465974643968,24.949970264493,-60.9744972704739));
#12846=CARTESIAN_POINT('Ctrl Pts',(-20.6756935485709,25.0087901934689,-60.9703753991033));
#12847=CARTESIAN_POINT('Ctrl Pts',(-20.7164230972664,25.0851686310756,-60.9648559333595));
#12848=CARTESIAN_POINT('Ctrl Pts',(-20.7264633803597,25.103562382356,-60.9635136245565));
#12849=CARTESIAN_POINT('Ctrl Pts',(-20.8622295329458,25.3466182758445,-60.9456012242814));
#12850=CARTESIAN_POINT('Ctrl Pts',(-21.0142424484423,25.5554980766441,-60.9280964250937));
#12851=CARTESIAN_POINT('Ctrl Pts',(-21.2988391175304,25.8617637471296,-60.8998792122918));
#12852=CARTESIAN_POINT('Ctrl Pts',(-21.4169086158251,25.9711622806561,-60.889152410606));
#12853=CARTESIAN_POINT('Ctrl Pts',(-21.5482032102938,26.0757160989634,-60.8785859244094));
#12854=CARTESIAN_POINT('Ctrl Pts',(-21.5537576880001,26.0801094557593,-60.8781413002778));
#12855=CARTESIAN_POINT('Ctrl Pts',(-21.5622560012386,26.086785842045,-60.87746473411));
#12856=CARTESIAN_POINT('Ctrl Pts',(-21.5651893445344,26.0890821011879,-60.8772318754741));
#12857=CARTESIAN_POINT('Ctrl Pts',(-21.5700007702767,26.0928351110924,-60.8768510338781));
#12858=CARTESIAN_POINT('Ctrl Pts',(-21.5718764842327,26.0942948714704,-60.8767028387621));
#12859=CARTESIAN_POINT('Ctrl Pts',(-21.5754975667027,26.0971065252749,-60.8764172783773));
#12860=CARTESIAN_POINT('Ctrl Pts',(-21.577242711934,26.0984587022339,-60.8762798929217));
#12861=CARTESIAN_POINT('Ctrl Pts',(-21.5804347946224,26.1009267531469,-60.8760290342565));
#12862=CARTESIAN_POINT('Ctrl Pts',(-21.5818812858526,26.1020431853049,-60.8759155212058));
#12863=CARTESIAN_POINT('Ctrl Pts',(-21.5848352594108,26.1043191175904,-60.875684042229));
#12864=CARTESIAN_POINT('Ctrl Pts',(-21.586342812897,26.1054785091455,-60.8755660840986));
#12865=CARTESIAN_POINT('Ctrl Pts',(-21.5906891729444,26.1088149804132,-60.8752265099603));
#12866=CARTESIAN_POINT('Ctrl Pts',(-21.5935305909549,26.1109886773902,-60.8750051351621));
#12867=CARTESIAN_POINT('Ctrl Pts',(-21.6060555433122,26.1205373004778,-60.8740320162764));
#12868=CARTESIAN_POINT('Ctrl Pts',(-21.6157773605267,26.1278621890223,-60.8732837754835));
#12869=CARTESIAN_POINT('Ctrl Pts',(-21.7674286975885,26.2407824014019,-60.8617175427094));
#12870=CARTESIAN_POINT('Ctrl Pts',(-21.9177699890985,26.3345669943791,-60.8516735527638));
#12871=CARTESIAN_POINT('Ctrl Pts',(-22.0750360359093,26.4155367851434,-60.8417499040898));
#12872=CARTESIAN_POINT('Origin',(-23.5502525316942,23.5502525316942,-77.3107734492734));
#12873=CARTESIAN_POINT('',(-22.0750359236218,26.4155367273312,-59.3465003279648));
#12874=CARTESIAN_POINT('',(-22.075036024144,26.4155367790859,-59.5958634867516));
#12875=CARTESIAN_POINT('',(-22.0750360153461,26.4155367745563,-77.3107734492734));
#12876=CARTESIAN_POINT('Ctrl Pts',(-22.0750359236218,26.4155367273312,-59.3465003279648));
#12877=CARTESIAN_POINT('Ctrl Pts',(-22.0173772946812,26.3858506783378,-59.350124039512));
#12878=CARTESIAN_POINT('Ctrl Pts',(-21.9606093800186,26.3544214700763,-59.3537501044204));
#12879=CARTESIAN_POINT('Ctrl Pts',(-21.7756671778268,26.2446027838705,-59.3658557842911));
#12880=CARTESIAN_POINT('Ctrl Pts',(-21.6520552993429,26.1589910297971,-59.3744380071984));
#12881=CARTESIAN_POINT('Ctrl Pts',(-21.4892612094151,26.0285278464637,-59.3868125885143));
#12882=CARTESIAN_POINT('Ctrl Pts',(-21.4446571477287,25.9907445260588,-59.3903248505198));
#12883=CARTESIAN_POINT('Ctrl Pts',(-21.3949405127218,25.9462525618812,-59.3943921134696));
#12884=CARTESIAN_POINT('Ctrl Pts',(-21.3887952442959,25.9407103197596,-59.3948975869124));
#12885=CARTESIAN_POINT('Ctrl Pts',(-21.3795669399565,25.9323228966746,-59.3956608194333));
#12886=CARTESIAN_POINT('Ctrl Pts',(-21.3764679690478,25.9294952340751,-59.3959178347945));
#12887=CARTESIAN_POINT('Ctrl Pts',(-21.3711359606365,25.9246109184007,-59.3963612841975));
#12888=CARTESIAN_POINT('Ctrl Pts',(-21.3689002863089,25.9225571411892,-59.3965475955051));
#12889=CARTESIAN_POINT('Ctrl Pts',(-21.3642911099066,25.9183109484524,-59.3969324831774));
#12890=CARTESIAN_POINT('Ctrl Pts',(-21.3619179970227,25.9161181168381,-59.3971310772339));
#12891=CARTESIAN_POINT('Ctrl Pts',(-21.3555131659794,25.910181968417,-59.3976682272017));
#12892=CARTESIAN_POINT('Ctrl Pts',(-21.3514877423232,25.9064319030814,-59.3980070724666));
#12893=CARTESIAN_POINT('Ctrl Pts',(-21.3366204468955,25.8925103232021,-59.3992631942189));
#12894=CARTESIAN_POINT('Ctrl Pts',(-21.3258395218915,25.8822742551436,-59.4001832531385));
#12895=CARTESIAN_POINT('Ctrl Pts',(-21.1474322168789,25.7105207081627,-59.4155643009805));
#12896=CARTESIAN_POINT('Ctrl Pts',(-20.9977551063138,25.5314187016644,-59.4308501551163));
#12897=CARTESIAN_POINT('Ctrl Pts',(-20.7974584960904,25.2309472079449,-59.4551849163107));
#12898=CARTESIAN_POINT('Ctrl Pts',(-20.7326787282184,25.1199300049788,-59.4639211022191));
#12899=CARTESIAN_POINT('Ctrl Pts',(-20.6269721687529,24.9110323577736,-59.4796514581286));
#12900=CARTESIAN_POINT('Ctrl Pts',(-20.5839126175309,24.8144207969308,-59.4866694885227));
#12901=CARTESIAN_POINT('Ctrl Pts',(-20.532087943081,24.6808327378886,-59.4958805012161));
#12902=CARTESIAN_POINT('Ctrl Pts',(-20.5191122908156,24.6455690312495,-59.4982667059051));
#12903=CARTESIAN_POINT('Ctrl Pts',(-20.5051994858254,24.6056159292935,-59.5009131986996));
#12904=CARTESIAN_POINT('Ctrl Pts',(-20.5036531952615,24.6011437901395,-59.5012086345051));
#12905=CARTESIAN_POINT('Ctrl Pts',(-20.5014987947507,24.5948681720328,-59.5016220754089));
#12906=CARTESIAN_POINT('Ctrl Pts',(-20.500882433883,24.5930675638004,-59.5017405695249));
#12907=CARTESIAN_POINT('Ctrl Pts',(-20.4996487926663,24.5894532151962,-59.501978157903));
#12908=CARTESIAN_POINT('Ctrl Pts',(-20.4990315331263,24.5876394658374,-59.5020972509772));
#12909=CARTESIAN_POINT('Ctrl Pts',(-20.4978529019578,24.5841660351013,-59.5023250642661));
#12910=CARTESIAN_POINT('Ctrl Pts',(-20.4972912671452,24.5825064487815,-59.5024338003034));
#12911=CARTESIAN_POINT('Ctrl Pts',(-20.4959729263132,24.5786003687439,-59.5026894650902));
#12912=CARTESIAN_POINT('Ctrl Pts',(-20.4952173437589,24.5763534927951,-59.5028363265975));
#12913=CARTESIAN_POINT('Ctrl Pts',(-20.4929974630942,24.5697280458566,-59.5032687891019));
#12914=CARTESIAN_POINT('Ctrl Pts',(-20.4915400862782,24.5653471358282,-59.5035539805623));
#12915=CARTESIAN_POINT('Ctrl Pts',(-20.4790977572962,24.5276751012545,-59.5059999460248));
#12916=CARTESIAN_POINT('Ctrl Pts',(-20.4686467288547,24.494208277285,-59.5081297389497));
#12917=CARTESIAN_POINT('Ctrl Pts',(-20.4569700849623,24.4545537417697,-59.5106100206929));
#12918=CARTESIAN_POINT('Ctrl Pts',(-20.4552143824401,24.4485263372307,-59.510985846726));
#12919=CARTESIAN_POINT('Ctrl Pts',(-20.4526237822133,24.4395349247291,-59.5115447954053));
#12920=CARTESIAN_POINT('Ctrl Pts',(-20.4517755126702,24.4365748245968,-59.5117285363789));
#12921=CARTESIAN_POINT('Ctrl Pts',(-20.4495975911602,24.4289334659643,-59.5122021620603));
#12922=CARTESIAN_POINT('Ctrl Pts',(-20.4482742929807,24.4242503873013,-59.5124917575672));
#12923=CARTESIAN_POINT('Ctrl Pts',(-20.4255545713473,24.3431449559493,-59.5174959003126));
#12924=CARTESIAN_POINT('Ctrl Pts',(-20.4069760578338,24.2659553555244,-59.5220850525385));
#12925=CARTESIAN_POINT('Ctrl Pts',(-20.3458825187809,23.9634104038351,-59.539675164646));
#12926=CARTESIAN_POINT('Ctrl Pts',(-20.3246116535162,23.734464818389,-59.5521875532458));
#12927=CARTESIAN_POINT('Ctrl Pts',(-20.3297447749188,23.3673664092994,-59.5731410623727));
#12928=CARTESIAN_POINT('Ctrl Pts',(-20.340512009612,23.2298212739769,-59.5811820196773));
#12929=CARTESIAN_POINT('Ctrl Pts',(-20.3631230207747,23.0719289624684,-59.5908230836809));
#12930=CARTESIAN_POINT('Ctrl Pts',(-20.366414161883,23.0504914333308,-59.5921407207343));
#12931=CARTESIAN_POINT('Ctrl Pts',(-20.3709128061222,23.023039046798,-59.5938396567481));
#12932=CARTESIAN_POINT('Ctrl Pts',(-20.3719214988249,23.0169918131557,-59.5942146232688));
#12933=CARTESIAN_POINT('Ctrl Pts',(-20.3735716445329,23.007270011344,-59.5948186130557));
#12934=CARTESIAN_POINT('Ctrl Pts',(-20.3742022358028,23.0035935941069,-59.5950472901148));
#12935=CARTESIAN_POINT('Ctrl Pts',(-20.3754133790688,22.9966053309944,-59.5954824861436));
#12936=CARTESIAN_POINT('Ctrl Pts',(-20.3759927344794,22.9932932804597,-59.5956889667109));
#12937=CARTESIAN_POINT('Ctrl Pts',(-20.3773224531287,22.9857610329246,-59.5961590508852));
#12938=CARTESIAN_POINT('Ctrl Pts',(-20.3780760537248,22.9815414205111,-59.5964227574375));
#12939=CARTESIAN_POINT('Ctrl Pts',(-20.3803890156649,22.9687381612904,-59.5972240105418));
#12940=CARTESIAN_POINT('Ctrl Pts',(-20.3819748058899,22.9601593839527,-59.597762399752));
#12941=CARTESIAN_POINT('Ctrl Pts',(-20.3887032756285,22.9245689526593,-59.600002355265));
#12942=CARTESIAN_POINT('Ctrl Pts',(-20.3941565953864,22.8976178675606,-59.6017138232034));
#12943=CARTESIAN_POINT('Ctrl Pts',(-20.4009929694648,22.8659236237925,-59.6037450658337));
#12944=CARTESIAN_POINT('Ctrl Pts',(-20.4020430041073,22.8611091398961,-59.6040541265554));
#12945=CARTESIAN_POINT('Ctrl Pts',(-20.4040925900449,22.8518140886933,-59.6046517958645));
#12946=CARTESIAN_POINT('Ctrl Pts',(-20.405090681758,22.8473332088307,-59.6049403572815));
#12947=CARTESIAN_POINT('Ctrl Pts',(-20.4078150672725,22.8352242013184,-59.605721357564));
#12948=CARTESIAN_POINT('Ctrl Pts',(-20.4095595525197,22.8276002364154,-59.606214372678));
#12949=CARTESIAN_POINT('Ctrl Pts',(-20.4128871468066,22.8132972279942,-59.6071417321269));
#12950=CARTESIAN_POINT('Ctrl Pts',(-20.4144638787303,22.8066167332564,-59.6075758724975));
#12951=CARTESIAN_POINT('Ctrl Pts',(-20.41739339725,22.7943795843902,-59.6083729590447));
#12952=CARTESIAN_POINT('Ctrl Pts',(-20.418739658501,22.7888213837297,-59.6087356987599));
#12953=CARTESIAN_POINT('Ctrl Pts',(-20.4210526448572,22.7793818356274,-59.6093529319674));
#12954=CARTESIAN_POINT('Ctrl Pts',(-20.422011817887,22.775498636521,-59.6096071889998));
#12955=CARTESIAN_POINT('Ctrl Pts',(-20.4243344821483,22.7661699964826,-59.610218817166));
#12956=CARTESIAN_POINT('Ctrl Pts',(-20.4257049732669,22.7607263263077,-59.6105764049872));
#12957=CARTESIAN_POINT('Ctrl Pts',(-20.4330324768955,22.7319389564394,-59.6124709962302));
#12958=CARTESIAN_POINT('Ctrl Pts',(-20.4392367652285,22.7086595008939,-59.6140155897627));
#12959=CARTESIAN_POINT('Ctrl Pts',(-20.4679670446683,22.6055205132541,-59.6209146518101));
#12960=CARTESIAN_POINT('Ctrl Pts',(-20.4933098080248,22.5264840878987,-59.6263519844875));
#12961=CARTESIAN_POINT('Ctrl Pts',(-20.5800073779294,22.2881593067768,-59.6431854392778));
#12962=CARTESIAN_POINT('Ctrl Pts',(-20.6509843749036,22.132693566,-59.6547961756307));
#12963=CARTESIAN_POINT('Ctrl Pts',(-20.8139310313397,21.8397712074789,-59.6774188571261));
#12964=CARTESIAN_POINT('Ctrl Pts',(-20.9048448057909,21.7022712749116,-59.6884001474609));
#12965=CARTESIAN_POINT('Ctrl Pts',(-21.0105154604079,21.5663396680548,-59.6992062730567));
#12966=CARTESIAN_POINT('Ctrl Pts',(-21.0151733744053,21.5603911518994,-59.6996790319789));
#12967=CARTESIAN_POINT('Ctrl Pts',(-21.0216212961037,21.5522160461993,-59.7003285061988));
#12968=CARTESIAN_POINT('Ctrl Pts',(-21.0233933624769,21.5499754353731,-59.7005064870392));
#12969=CARTESIAN_POINT('Ctrl Pts',(-21.0263900024129,21.5461968037248,-59.7008065920719));
#12970=CARTESIAN_POINT('Ctrl Pts',(-21.0276130041124,21.5446575472947,-59.700928829088));
#12971=CARTESIAN_POINT('Ctrl Pts',(-21.0300261651114,21.5416260689448,-59.7011695402527));
#12972=CARTESIAN_POINT('Ctrl Pts',(-21.0312162416839,21.5401337851218,-59.7012880200473));
#12973=CARTESIAN_POINT('Ctrl Pts',(-21.0338451188819,21.5368433336492,-59.7015492379908));
#12974=CARTESIAN_POINT('Ctrl Pts',(-21.0352845250735,21.5350456460915,-59.701691932395));
#12975=CARTESIAN_POINT('Ctrl Pts',(-21.0403300869684,21.5287580232355,-59.702190965878));
#12976=CARTESIAN_POINT('Ctrl Pts',(-21.0439463771026,21.5242761777013,-59.7025465774121));
#12977=CARTESIAN_POINT('Ctrl Pts',(-21.0811029248206,21.4784779870898,-59.7061796672845));
#12978=CARTESIAN_POINT('Ctrl Pts',(-21.1156520445821,21.4379857814073,-59.7093854868471));
#12979=CARTESIAN_POINT('Ctrl Pts',(-21.1666304013744,21.3811518463552,-59.7139068521463));
#12980=CARTESIAN_POINT('Ctrl Pts',(-21.1822553380077,21.3641048729292,-59.7152659288294));
#12981=CARTESIAN_POINT('Ctrl Pts',(-21.3721402340304,21.1613630841721,-59.7314860823134));
#12982=CARTESIAN_POINT('Ctrl Pts',(-21.5676463071214,20.9967720227785,-59.7452950057434));
#12983=CARTESIAN_POINT('Ctrl Pts',(-21.8875410813069,20.7865755134584,-59.7669743011235));
#12984=CARTESIAN_POINT('Ctrl Pts',(-21.9986615908709,20.7226951837666,-59.7743510430123));
#12985=CARTESIAN_POINT('Ctrl Pts',(-22.1615829599092,20.641536920671,-59.785170828009));
#12986=CARTESIAN_POINT('Ctrl Pts',(-22.2104800701052,20.6186934063143,-59.7884176983647));
#12987=CARTESIAN_POINT('Ctrl Pts',(-22.2673669239226,20.5938378066815,-59.7922026749949));
#12988=CARTESIAN_POINT('Ctrl Pts',(-22.2748205622714,20.5906145811383,-59.7926987466116));
#12989=CARTESIAN_POINT('Ctrl Pts',(-22.2861136737287,20.5857816105326,-59.79345059514));
#12990=CARTESIAN_POINT('Ctrl Pts',(-22.2899442533509,20.5841510604171,-59.7937056614641));
#12991=CARTESIAN_POINT('Ctrl Pts',(-22.2965696188065,20.5813460146907,-59.7941469008554));
#12992=CARTESIAN_POINT('Ctrl Pts',(-22.2993629288236,20.580168028839,-59.7943329547171));
#12993=CARTESIAN_POINT('Ctrl Pts',(-22.3051490847142,20.5777375199939,-59.7947184035978));
#12994=CARTESIAN_POINT('Ctrl Pts',(-22.3081421672274,20.5764855719579,-59.7949178179378));
#12995=CARTESIAN_POINT('Ctrl Pts',(-22.3154024569013,20.5734616078253,-59.7954016057109));
#12996=CARTESIAN_POINT('Ctrl Pts',(-22.3196715856441,20.5716942484779,-59.7956861370568));
#12997=CARTESIAN_POINT('Ctrl Pts',(-22.3356022460903,20.5651392743798,-59.7967481231989));
#12998=CARTESIAN_POINT('Ctrl Pts',(-22.3472879177742,20.5604109630301,-59.7975275855451));
#12999=CARTESIAN_POINT('Ctrl Pts',(-22.5467118902965,20.4810775042744,-59.8108383730785));
#13000=CARTESIAN_POINT('Ctrl Pts',(-22.7409909711201,20.424233167802,-59.8239812598038));
#13001=CARTESIAN_POINT('Ctrl Pts',(-23.2295720225636,20.3298964066313,-59.8573012705182));
#13002=CARTESIAN_POINT('Ctrl Pts',(-23.5261978870492,20.3140568723038,-59.8778263065868));
#13003=CARTESIAN_POINT('Ctrl Pts',(-23.8290318680961,20.3395723205871,-59.8969911380142));
#13004=CARTESIAN_POINT('Ctrl Pts',(-23.8372327183176,20.340294944383,-59.8975086596434));
#13005=CARTESIAN_POINT('Ctrl Pts',(-23.8514210754071,20.3415999706347,-59.898401380229));
#13006=CARTESIAN_POINT('Ctrl Pts',(-23.8574098409415,20.3421677232635,-59.8987773716775));
#13007=CARTESIAN_POINT('Ctrl Pts',(-23.8659813534834,20.3430045500236,-59.8993143109849));
#13008=CARTESIAN_POINT('Ctrl Pts',(-23.868565373045,20.3432599779168,-59.8994760231683));
#13009=CARTESIAN_POINT('Ctrl Pts',(-23.8730522516803,20.3437089780271,-59.899756543793));
#13010=CARTESIAN_POINT('Ctrl Pts',(-23.8749552498663,20.3439011214975,-59.8998754335152));
#13011=CARTESIAN_POINT('Ctrl Pts',(-23.878604846555,20.3442728994038,-59.9001032753092));
#13012=CARTESIAN_POINT('Ctrl Pts',(-23.8803514664438,20.3444522667605,-59.9002122425116));
#13013=CARTESIAN_POINT('Ctrl Pts',(-23.8844705725032,20.3448786762148,-59.9004690526229));
#13014=CARTESIAN_POINT('Ctrl Pts',(-23.886842936682,20.3451269254895,-59.9006168267895));
#13015=CARTESIAN_POINT('Ctrl Pts',(-23.8938635855557,20.3458694620634,-59.9010537526299));
#13016=CARTESIAN_POINT('Ctrl Pts',(-23.8985110984906,20.3463712316807,-59.9013424827232));
#13017=CARTESIAN_POINT('Ctrl Pts',(-23.9395100435417,20.3508879548782,-59.9038852438706));
#13018=CARTESIAN_POINT('Ctrl Pts',(-23.9757936397396,20.3555115172861,-59.9061055304805));
#13019=CARTESIAN_POINT('Ctrl Pts',(-24.0154195319105,20.3612481079009,-59.9085051064685));
#13020=CARTESIAN_POINT('Ctrl Pts',(-24.0188457588702,20.3617497575513,-59.9087123771234));
#13021=CARTESIAN_POINT('Ctrl Pts',(-24.3042021182704,20.4039999804145,-59.9259583351109));
#13022=CARTESIAN_POINT('Ctrl Pts',(-24.5793887752279,20.4829618592487,-59.9413170874108));
#13023=CARTESIAN_POINT('Ctrl Pts',(-25.0067341873305,20.6696904647225,-59.9676834281384));
#13024=CARTESIAN_POINT('Ctrl Pts',(-25.166395609331,20.756143809207,-59.9781710891231));
#13025=CARTESIAN_POINT('Ctrl Pts',(-25.329147680033,20.8629063402261,-59.9899946634912));
#13026=CARTESIAN_POINT('Ctrl Pts',(-25.3403177347086,20.8703338646422,-59.9908120852706));
#13027=CARTESIAN_POINT('Ctrl Pts',(-25.3556755254798,20.8806848788377,-59.9919443240949));
#13028=CARTESIAN_POINT('Ctrl Pts',(-25.3599032793545,20.8835489841125,-59.9922568923907));
#13029=CARTESIAN_POINT('Ctrl Pts',(-25.3670217852286,20.8883961623719,-59.9927846769584));
#13030=CARTESIAN_POINT('Ctrl Pts',(-25.3699161511782,20.8903739323477,-59.9929996914498));
#13031=CARTESIAN_POINT('Ctrl Pts',(-25.3756316117088,20.8942930997055,-59.9934251086096));
#13032=CARTESIAN_POINT('Ctrl Pts',(-25.3784528505917,20.896234279316,-59.9936355027935));
#13033=CARTESIAN_POINT('Ctrl Pts',(-25.3846574087252,20.9005179706721,-59.9940990966014));
#13034=CARTESIAN_POINT('Ctrl Pts',(-25.3880393425899,20.9028624708601,-59.9943523720317));
#13035=CARTESIAN_POINT('Ctrl Pts',(-25.3998000234784,20.911048869701,-59.9952351785167));
#13036=CARTESIAN_POINT('Ctrl Pts',(-25.4081554139133,20.9169240732162,-59.9958659852791));
#13037=CARTESIAN_POINT('Ctrl Pts',(-25.4918449343839,20.9763680446748,-60.0022210463195));
#13038=CARTESIAN_POINT('Ctrl Pts',(-25.564862227215,21.0331098364371,-60.0080681703204));
#13039=CARTESIAN_POINT('Ctrl Pts',(-25.8625881822234,21.2857332249386,-60.033265499888));
#13040=CARTESIAN_POINT('Ctrl Pts',(-26.0619745368346,21.509140078756,-60.0537745390458));
#13041=CARTESIAN_POINT('Ctrl Pts',(-26.2938834700108,21.8553453428623,-60.0816122387195));
#13042=CARTESIAN_POINT('Ctrl Pts',(-26.3544812706904,21.9576039424041,-60.0894035845731));
#13043=CARTESIAN_POINT('Ctrl Pts',(-26.4122045720747,22.0685684679297,-60.0972425865282));
#13044=CARTESIAN_POINT('Ctrl Pts',(-26.4150917408016,22.0741585462706,-60.0976358944136));
#13045=CARTESIAN_POINT('Ctrl Pts',(-26.4191728718421,22.0821174287764,-60.0981935588825));
#13046=CARTESIAN_POINT('Ctrl Pts',(-26.4203802847927,22.0844792615227,-60.0983587600566));
#13047=CARTESIAN_POINT('Ctrl Pts',(-26.4224535132973,22.088547108621,-60.0986427911945));
#13048=CARTESIAN_POINT('Ctrl Pts',(-26.4233207268836,22.0902524055211,-60.0987617101218));
#13049=CARTESIAN_POINT('Ctrl Pts',(-26.4249806749187,22.0935237491325,-60.0989895469787));
#13050=CARTESIAN_POINT('Ctrl Pts',(-26.4257736471919,22.0950896687285,-60.0990984801395));
#13051=CARTESIAN_POINT('Ctrl Pts',(-26.4276402372848,22.0987831956224,-60.0993551221038));
#13052=CARTESIAN_POINT('Ctrl Pts',(-26.4287127770296,22.1009113510366,-60.0995027623849));
#13053=CARTESIAN_POINT('Ctrl Pts',(-26.4318782871194,22.1072097950077,-60.0999390323621));
#13054=CARTESIAN_POINT('Ctrl Pts',(-26.433964573851,22.1113834644054,-60.1002272422594));
#13055=CARTESIAN_POINT('Ctrl Pts',(-26.4522220110156,22.148107136472,-60.1027555306236));
#13056=CARTESIAN_POINT('Ctrl Pts',(-26.4678513356023,22.1809256676392,-60.1049622855749));
#13057=CARTESIAN_POINT('Ctrl Pts',(-26.4875046542662,22.2240588660547,-60.1078034809899));
#13058=CARTESIAN_POINT('Ctrl Pts',(-26.4920347311562,22.2341381111733,-60.1084632455988));
#13059=CARTESIAN_POINT('Ctrl Pts',(-26.4970653730707,22.2454868444057,-60.1092016646997));
#13060=CARTESIAN_POINT('Ctrl Pts',(-26.4976170187264,22.2467334480492,-60.1092827164232));
#13061=CARTESIAN_POINT('Ctrl Pts',(-26.5019604704807,22.2565655928052,-60.1099215126411));
#13062=CARTESIAN_POINT('Ctrl Pts',(-26.5057155851707,22.2651674002527,-60.1104775456415));
#13063=CARTESIAN_POINT('Ctrl Pts',(-26.5117820533869,22.2792310427963,-60.1113822254147));
#13064=CARTESIAN_POINT('Ctrl Pts',(-26.5141159779098,22.2846830131811,-60.1117318594899));
#13065=CARTESIAN_POINT('Ctrl Pts',(-26.5188165865334,22.2957478011878,-60.112439320364));
#13066=CARTESIAN_POINT('Ctrl Pts',(-26.5211824337836,22.3013609493878,-60.1127971108396));
#13067=CARTESIAN_POINT('Ctrl Pts',(-26.5695746344609,22.4170907223686,-60.1201518664266));
#13068=CARTESIAN_POINT('Ctrl Pts',(-26.609468438359,22.5296820879871,-60.1268991887596));
#13069=CARTESIAN_POINT('Ctrl Pts',(-26.6906262705954,22.8067216855026,-60.1430863782956));
#13070=CARTESIAN_POINT('Ctrl Pts',(-26.7253460501128,22.9727018429127,-60.1524562065995));
#13071=CARTESIAN_POINT('Ctrl Pts',(-26.7642594881813,23.2763815102056,-60.1699360504974));
#13072=CARTESIAN_POINT('Ctrl Pts',(-26.7729877313807,23.4130779017761,-60.1779220034576));
#13073=CARTESIAN_POINT('Ctrl Pts',(-26.7730047994707,23.571070348832,-60.1874722551341));
#13074=CARTESIAN_POINT('Ctrl Pts',(-26.7727985692626,23.592235427216,-60.188758054415));
#13075=CARTESIAN_POINT('Ctrl Pts',(-26.7722595413803,23.6197410970653,-60.1904378740434));
#13076=CARTESIAN_POINT('Ctrl Pts',(-26.772116469424,23.6260852227331,-60.190825930829));
#13077=CARTESIAN_POINT('Ctrl Pts',(-26.7718583211161,23.6362058631113,-60.1914459760378));
#13078=CARTESIAN_POINT('Ctrl Pts',(-26.7717553387269,23.63998269221,-60.1916775843502));
#13079=CARTESIAN_POINT('Ctrl Pts',(-26.7715581395575,23.6467763815224,-60.1920945947429));
#13080=CARTESIAN_POINT('Ctrl Pts',(-26.7714663255739,23.649793311557,-60.1922799211158));
#13081=CARTESIAN_POINT('Ctrl Pts',(-26.7712414441191,23.6568563655759,-60.1927141284065));
#13082=CARTESIAN_POINT('Ctrl Pts',(-26.7711049909629,23.6609023701423,-60.1929631154232));
#13083=CARTESIAN_POINT('Ctrl Pts',(-26.770691293151,23.6725192104432,-60.1936787432422));
#13084=CARTESIAN_POINT('Ctrl Pts',(-26.7703949770755,23.6800893019452,-60.1941459824795));
#13085=CARTESIAN_POINT('Ctrl Pts',(-26.7682767490844,23.7297256118591,-60.19721561773));
#13086=CARTESIAN_POINT('Ctrl Pts',(-26.7656573484119,23.7717520655879,-60.1998429676425));
#13087=CARTESIAN_POINT('Ctrl Pts',(-26.755477368879,23.8958604127444,-60.2076902056564));
#13088=CARTESIAN_POINT('Ctrl Pts',(-26.7455909387516,23.977711981398,-60.2129812406296));
#13089=CARTESIAN_POINT('Ctrl Pts',(-26.6857718821446,24.3518276798081,-60.2376999764782));
#13090=CARTESIAN_POINT('Ctrl Pts',(-26.598809266847,24.6366520507987,-60.2582056246918));
#13091=CARTESIAN_POINT('Ctrl Pts',(-26.4354853541177,24.9890052290981,-60.2839142862488));
#13092=CARTESIAN_POINT('Ctrl Pts',(-26.3932447932339,25.0707710293686,-60.289890800783));
#13093=CARTESIAN_POINT('Ctrl Pts',(-26.3443587414358,25.1562194005458,-60.2960624935213));
#13094=CARTESIAN_POINT('Ctrl Pts',(-26.3411416456934,25.1618036634371,-60.2964654772798));
#13095=CARTESIAN_POINT('Ctrl Pts',(-26.3366619136796,25.1695259746961,-60.297022223029));
#13096=CARTESIAN_POINT('Ctrl Pts',(-26.3354135530036,25.1716722221841,-60.2971769016029));
#13097=CARTESIAN_POINT('Ctrl Pts',(-26.3332653111698,25.1753557914515,-60.297442273519));
#13098=CARTESIAN_POINT('Ctrl Pts',(-26.3323666359851,25.1768938094011,-60.2975530453968));
#13099=CARTESIAN_POINT('Ctrl Pts',(-26.3305093130978,25.1800664422091,-60.2977814828632));
#13100=CARTESIAN_POINT('Ctrl Pts',(-26.3295505007262,25.1817009534339,-60.2978991367286));
#13101=CARTESIAN_POINT('Ctrl Pts',(-26.3272988317732,25.1855316835662,-60.2981747965668));
#13102=CARTESIAN_POINT('Ctrl Pts',(-26.3260048073851,25.1877272220128,-60.2983327259834));
#13103=CARTESIAN_POINT('Ctrl Pts',(-26.3218055176039,25.1948327691431,-60.298843649404));
#13104=CARTESIAN_POINT('Ctrl Pts',(-26.3188897972028,25.1997366341733,-60.2991959629041));
#13105=CARTESIAN_POINT('Ctrl Pts',(-26.2439788408215,25.3249689503363,-60.3081862023098));
#13106=CARTESIAN_POINT('Ctrl Pts',(-26.1642085689124,25.440497239046,-60.3163174272702));
#13107=CARTESIAN_POINT('Ctrl Pts',(-25.9684216888671,25.6878367757681,-60.3342158289763));
#13108=CARTESIAN_POINT('Ctrl Pts',(-25.8486691711063,25.8161061001435,-60.3438666105886));
#13109=CARTESIAN_POINT('Ctrl Pts',(-25.57808522971,26.0622933616988,-60.3645060287927));
#13110=CARTESIAN_POINT('Ctrl Pts',(-25.4260072723916,26.1777955466537,-60.3755059068929));
#13111=CARTESIAN_POINT('Ctrl Pts',(-25.253945890953,26.2858887857408,-60.3878533271851));
#13112=CARTESIAN_POINT('Ctrl Pts',(-25.2432221417095,26.2925381968471,-60.3886223592442));
#13113=CARTESIAN_POINT('Ctrl Pts',(-25.2285170554604,26.3015371620069,-60.3896762934858));
#13114=CARTESIAN_POINT('Ctrl Pts',(-25.2245692029949,26.3039414416058,-60.3899591817206));
#13115=CARTESIAN_POINT('Ctrl Pts',(-25.2178411971761,26.3080190436573,-60.3904411891045));
#13116=CARTESIAN_POINT('Ctrl Pts',(-25.2150636556672,26.3096966809984,-60.390640149753));
#13117=CARTESIAN_POINT('Ctrl Pts',(-25.2096864230587,26.3129334600724,-60.391025279687));
#13118=CARTESIAN_POINT('Ctrl Pts',(-25.2070870559778,26.3144931346225,-60.3912114291561));
#13119=CARTESIAN_POINT('Ctrl Pts',(-25.2009136280183,26.3181854842478,-60.3916534761466));
#13120=CARTESIAN_POINT('Ctrl Pts',(-25.1973376352752,26.3203149039257,-60.3919094922262));
#13121=CARTESIAN_POINT('Ctrl Pts',(-25.187389247819,26.3262128600497,-60.392621616398));
#13122=CARTESIAN_POINT('Ctrl Pts',(-25.1810080070895,26.3299663568729,-60.3930782715522));
#13123=CARTESIAN_POINT('Ctrl Pts',(-25.1663696653526,26.3385089919616,-60.3941255610623));
#13124=CARTESIAN_POINT('Ctrl Pts',(-25.1581041365088,26.3432834824119,-60.3947167229978));
#13125=CARTESIAN_POINT('Ctrl Pts',(-25.0893885365455,26.3825701740473,-60.3996299771872));
#13126=CARTESIAN_POINT('Ctrl Pts',(-25.0278601885118,26.4151499580849,-60.4040211240789));
#13127=CARTESIAN_POINT('Ctrl Pts',(-24.8978192591042,26.4787039343361,-60.4132943285966));
#13128=CARTESIAN_POINT('Ctrl Pts',(-24.8291807819336,26.5093241518804,-60.418184891596));
#13129=CARTESIAN_POINT('Ctrl Pts',(-24.5069543350152,26.6397659697369,-60.4411058036661));
#13130=CARTESIAN_POINT('Ctrl Pts',(-24.2424546628898,26.7095571241782,-60.459933690785));
#13131=CARTESIAN_POINT('Ctrl Pts',(-23.8870817229542,26.7565058974879,-60.4836035599354));
#13132=CARTESIAN_POINT('Ctrl Pts',(-23.8013906742619,26.7643538537402,-60.4891789756621));
#13133=CARTESIAN_POINT('Ctrl Pts',(-23.7091400280099,26.7690896859965,-60.4949693496883));
#13134=CARTESIAN_POINT('Ctrl Pts',(-23.7027991443989,26.7693964233187,-60.49536627816));
#13135=CARTESIAN_POINT('Ctrl Pts',(-23.693992967616,26.769796340248,-60.4959159982108));
#13136=CARTESIAN_POINT('Ctrl Pts',(-23.6915284654991,26.7699054258342,-60.49606967668));
#13137=CARTESIAN_POINT('Ctrl Pts',(-23.6872884155098,26.7700882242422,-60.4963337833273));
#13138=CARTESIAN_POINT('Ctrl Pts',(-23.6855129323779,26.7701632982374,-60.4964442883717));
#13139=CARTESIAN_POINT('Ctrl Pts',(-23.6818415228435,26.7703154969747,-60.496672613077));
#13140=CARTESIAN_POINT('Ctrl Pts',(-23.6799455938099,26.770392415708,-60.496790420385));
#13141=CARTESIAN_POINT('Ctrl Pts',(-23.6754879096935,26.7705693228126,-60.4970671733987));
#13142=CARTESIAN_POINT('Ctrl Pts',(-23.6729260943449,26.7706679291543,-60.4972260407615));
#13143=CARTESIAN_POINT('Ctrl Pts',(-23.6650823217219,26.7709604691473,-60.4977119126421));
#13144=CARTESIAN_POINT('Ctrl Pts',(-23.6597999689935,26.771144467009,-60.4980383592537));
#13145=CARTESIAN_POINT('Ctrl Pts',(-23.6091585005105,26.7727837125394,-60.5011608790759));
#13146=CARTESIAN_POINT('Ctrl Pts',(-23.5637710429255,26.7732937804024,-60.5039048788171));
#13147=CARTESIAN_POINT('Ctrl Pts',(-23.4316856831945,26.7719876234891,-60.5117707696838));
#13148=CARTESIAN_POINT('Ctrl Pts',(-23.3450491470703,26.7676317440791,-60.516780522324));
#13149=CARTESIAN_POINT('Ctrl Pts',(-22.9996077453542,26.7362506787536,-60.5365195067012));
#13150=CARTESIAN_POINT('Ctrl Pts',(-22.7443348990544,26.6814339857662,-60.5506546108481));
#13151=CARTESIAN_POINT('Ctrl Pts',(-22.3876945332645,26.5582915452666,-60.5724532544106));
#13152=CARTESIAN_POINT('Ctrl Pts',(-22.2791458531908,26.5140546117124,-60.5793712569388));
#13153=CARTESIAN_POINT('Ctrl Pts',(-22.1636614016266,26.4594784025496,-60.5871435566016));
#13154=CARTESIAN_POINT('Ctrl Pts',(-22.1540914150784,26.4548978218904,-60.5877907738047));
#13155=CARTESIAN_POINT('Ctrl Pts',(-22.1406816849293,26.448397803392,-60.5887021543608));
#13156=CARTESIAN_POINT('Ctrl Pts',(-22.1368228185175,26.4465177877668,-60.5889649423587));
#13157=CARTESIAN_POINT('Ctrl Pts',(-22.1301323527134,26.4432416790613,-60.5894214757179));
#13158=CARTESIAN_POINT('Ctrl Pts',(-22.1272990203828,26.4418491207902,-60.5896150973198));
#13159=CARTESIAN_POINT('Ctrl Pts',(-22.1214074079428,26.4389426881056,-60.5900183087608));
#13160=CARTESIAN_POINT('Ctrl Pts',(-22.1183494786592,26.4374281158915,-60.590227922842));
#13161=CARTESIAN_POINT('Ctrl Pts',(-22.1111535680511,26.4338497846713,-60.5907219782565));
#13162=CARTESIAN_POINT('Ctrl Pts',(-22.1070176196294,26.4317819750241,-60.591006561504));
#13163=CARTESIAN_POINT('Ctrl Pts',(-22.0937172089254,26.4250964799109,-60.5919237277604));
#13164=CARTESIAN_POINT('Ctrl Pts',(-22.0845704170188,26.420443955255,-60.5925575356074));
#13165=CARTESIAN_POINT('Ctrl Pts',(-22.0753093910179,26.4156775120256,-60.5932024084344));
#13166=CARTESIAN_POINT('Ctrl Pts',(-22.0751727006468,26.4156071481723,-60.5932119272902));
#13167=CARTESIAN_POINT('Ctrl Pts',(-22.0750360153461,26.4155367745563,-60.593221446491));
#13168=CARTESIAN_POINT('Ctrl Pts',(-22.0750360359093,26.4155367851434,-60.8417499040898));
#13169=CARTESIAN_POINT('Ctrl Pts',(-22.0927192681594,26.4246411509259,-60.8406340740182));
#13170=CARTESIAN_POINT('Ctrl Pts',(-22.1104900562006,26.4335835030538,-60.839519893482));
#13171=CARTESIAN_POINT('Ctrl Pts',(-22.2568456387877,26.5055392472628,-60.8303944504889));
#13172=CARTESIAN_POINT('Ctrl Pts',(-22.3894109364369,26.5600808014567,-60.8224390301533));
#13173=CARTESIAN_POINT('Ctrl Pts',(-22.6334616486051,26.6419610843305,-60.8077854404577));
#13174=CARTESIAN_POINT('Ctrl Pts',(-22.7436098978314,26.6725099112073,-60.8011705620584));
#13175=CARTESIAN_POINT('Ctrl Pts',(-22.90431647976,26.7080081401775,-60.7913698206017));
#13176=CARTESIAN_POINT('Ctrl Pts',(-22.9537383935735,26.7177159198882,-60.7883365259711));
#13177=CARTESIAN_POINT('Ctrl Pts',(-23.0111952847516,26.7276096049513,-60.7847813656634));
#13178=CARTESIAN_POINT('Ctrl Pts',(-23.0190300153356,26.7289288792939,-60.7842959788782));
#13179=CARTESIAN_POINT('Ctrl Pts',(-23.0309413614435,26.7308893390389,-60.7835570786854));
#13180=CARTESIAN_POINT('Ctrl Pts',(-23.0350145018689,26.731551694639,-60.7833042390555));
#13181=CARTESIAN_POINT('Ctrl Pts',(-23.042393777088,26.7327371352749,-60.7828458609202));
#13182=CARTESIAN_POINT('Ctrl Pts',(-23.0456994810719,26.7332628969978,-60.782640407828));
#13183=CARTESIAN_POINT('Ctrl Pts',(-23.0523048490332,26.7343029113359,-60.7822296493488));
#13184=CARTESIAN_POINT('Ctrl Pts',(-23.0556045052754,26.7348171871207,-60.7820243449691));
#13185=CARTESIAN_POINT('Ctrl Pts',(-23.0648771112009,26.736247632011,-60.7814470822878));
#13186=CARTESIAN_POINT('Ctrl Pts',(-23.0708518238472,26.7371521282585,-60.7810747537788));
#13187=CARTESIAN_POINT('Ctrl Pts',(-23.0953239310677,26.7407865210537,-60.7795481549777));
#13188=CARTESIAN_POINT('Ctrl Pts',(-23.1138420805997,26.7433721760827,-60.7783893194858));
#13189=CARTESIAN_POINT('Ctrl Pts',(-23.4383956353691,26.7858130160086,-60.7580125553829));
#13190=CARTESIAN_POINT('Ctrl Pts',(-23.7485055184797,26.7816558253434,-60.7372695635844));
#13191=CARTESIAN_POINT('Ctrl Pts',(-24.2333667577107,26.7050495521258,-60.7040649850076));
#13192=CARTESIAN_POINT('Ctrl Pts',(-24.4108199851544,26.6613343871955,-60.6918006109792));
#13193=CARTESIAN_POINT('Ctrl Pts',(-24.5907718854211,26.6004154369603,-60.6798320249399));
#13194=CARTESIAN_POINT('Ctrl Pts',(-24.5978965488266,26.5979756638311,-60.6793589805478));
#13195=CARTESIAN_POINT('Ctrl Pts',(-24.6086933441368,26.5942360700172,-60.6786434343658));
#13196=CARTESIAN_POINT('Ctrl Pts',(-24.6123717192506,26.5929545491167,-60.6783998853275));
#13197=CARTESIAN_POINT('Ctrl Pts',(-24.6183581414582,26.590856741734,-60.6780039056552));
#13198=CARTESIAN_POINT('Ctrl Pts',(-24.6206675841346,26.5900444935438,-60.677851238634));
#13199=CARTESIAN_POINT('Ctrl Pts',(-24.6251060742812,26.5884777581261,-60.6775580137381));
#13200=CARTESIAN_POINT('Ctrl Pts',(-24.6272352572321,26.5877236629986,-60.6774174326741));
#13201=CARTESIAN_POINT('Ctrl Pts',(-24.6310881323303,26.586354525411,-60.6771631933103));
#13202=CARTESIAN_POINT('Ctrl Pts',(-24.6328120889593,26.5857402547598,-60.6770494892484));
#13203=CARTESIAN_POINT('Ctrl Pts',(-24.6365584671785,26.5844017685712,-60.6768025146374));
#13204=CARTESIAN_POINT('Ctrl Pts',(-24.6385806829775,26.5836770012168,-60.6766692780056));
#13205=CARTESIAN_POINT('Ctrl Pts',(-24.6440286018754,26.5817183040162,-60.6763105324101));
#13206=CARTESIAN_POINT('Ctrl Pts',(-24.6474529539174,26.5804805848686,-60.6760852503993));
#13207=CARTESIAN_POINT('Ctrl Pts',(-24.6632263122969,26.5747491207523,-60.6750484933949));
#13208=CARTESIAN_POINT('Ctrl Pts',(-24.6755500875459,26.5701855902724,-60.6742411414979));
#13209=CARTESIAN_POINT('Ctrl Pts',(-24.8877205342354,26.4901391111063,-60.660382017347));
#13210=CARTESIAN_POINT('Ctrl Pts',(-25.0796376890542,26.3950311487297,-60.6484486051454));
#13211=CARTESIAN_POINT('Ctrl Pts',(-25.3307970859547,26.2377437785704,-60.6318868911879));
#13212=CARTESIAN_POINT('Ctrl Pts',(-25.3991285103761,26.1912003640066,-60.627275931628));
#13213=CARTESIAN_POINT('Ctrl Pts',(-25.5431664239775,26.0847574855856,-60.6171916598343));
#13214=CARTESIAN_POINT('Ctrl Pts',(-25.6181218344529,26.0239816917159,-60.6117075773721));
#13215=CARTESIAN_POINT('Ctrl Pts',(-25.7630241788694,25.8952975022938,-60.6004635560897));
#13216=CARTESIAN_POINT('Ctrl Pts',(-25.8328401377376,25.8273966358836,-60.5947073357034));
#13217=CARTESIAN_POINT('Ctrl Pts',(-25.9114499434178,25.7436905866326,-60.5877495252233));
#13218=CARTESIAN_POINT('Ctrl Pts',(-25.9233237799796,25.7308388174674,-60.5866849576331));
#13219=CARTESIAN_POINT('Ctrl Pts',(-25.9389019295051,25.7136997114076,-60.5852698408547));
#13220=CARTESIAN_POINT('Ctrl Pts',(-25.9427005892125,25.7094982186185,-60.584923298994));
#13221=CARTESIAN_POINT('Ctrl Pts',(-25.9489128860062,25.7025906128873,-60.584354135557));
#13222=CARTESIAN_POINT('Ctrl Pts',(-25.9513330781396,25.6998903896631,-60.5841317909482));
#13223=CARTESIAN_POINT('Ctrl Pts',(-25.9560093564078,25.6946552873362,-60.5837009933367));
#13224=CARTESIAN_POINT('Ctrl Pts',(-25.9582660070903,25.6921209170605,-60.5834925644841));
#13225=CARTESIAN_POINT('Ctrl Pts',(-25.9634602903801,25.6862688034178,-60.5830115664395));
#13226=CARTESIAN_POINT('Ctrl Pts',(-25.9663950863062,25.6829485614017,-60.5827388789108));
#13227=CARTESIAN_POINT('Ctrl Pts',(-25.9755075467889,25.6725963508094,-60.5818893097434));
#13228=CARTESIAN_POINT('Ctrl Pts',(-25.9816613887912,25.6655435616574,-60.5813114360234));
#13229=CARTESIAN_POINT('Ctrl Pts',(-26.0336203652701,25.6054681594473,-60.5763967421438));
#13230=CARTESIAN_POINT('Ctrl Pts',(-26.0777126612788,25.5509951743469,-60.5719898312863));
#13231=CARTESIAN_POINT('Ctrl Pts',(-26.1249876428917,25.4885314563594,-60.5669843921494));
#13232=CARTESIAN_POINT('Ctrl Pts',(-26.1299576138408,25.4819118623706,-60.5664545329812));
#13233=CARTESIAN_POINT('Ctrl Pts',(-26.1678212242771,25.4310738845209,-60.5623897662699));
#13234=CARTESIAN_POINT('Ctrl Pts',(-26.1995996749937,25.3860395513904,-60.5588148302716));
#13235=CARTESIAN_POINT('Ctrl Pts',(-26.3843285365374,25.1094611493674,-60.5370197063914));
#13236=CARTESIAN_POINT('Ctrl Pts',(-26.5079799767612,24.8598079628611,-60.5178710316903));
#13237=CARTESIAN_POINT('Ctrl Pts',(-26.6215600516023,24.5292256698858,-60.4946706302153));
#13238=CARTESIAN_POINT('Ctrl Pts',(-26.6426989019656,24.4602499775515,-60.4899486008065));
#13239=CARTESIAN_POINT('Ctrl Pts',(-26.6692963748976,24.3617791346785,-60.483426596055));
#13240=CARTESIAN_POINT('Ctrl Pts',(-26.6766849165052,24.3328320001674,-60.4815357431533));
#13241=CARTESIAN_POINT('Ctrl Pts',(-26.6847227585383,24.2994082059577,-60.4793860443901));
#13242=CARTESIAN_POINT('Ctrl Pts',(-26.6857661524543,24.2950291168983,-60.4791050574206));
#13243=CARTESIAN_POINT('Ctrl Pts',(-26.6873318084808,24.2883965044521,-60.4786804860559));
#13244=CARTESIAN_POINT('Ctrl Pts',(-26.6878608199647,24.2861446045012,-60.4785365127102));
#13245=CARTESIAN_POINT('Ctrl Pts',(-26.6888122277527,24.2820749687091,-60.4782766458007));
#13246=CARTESIAN_POINT('Ctrl Pts',(-26.6892354686168,24.2802574404497,-60.4781607034631));
#13247=CARTESIAN_POINT('Ctrl Pts',(-26.6901443653973,24.2763389487156,-60.4779109885361));
#13248=CARTESIAN_POINT('Ctrl Pts',(-26.6906294901014,24.2742378709857,-60.4777772472806));
#13249=CARTESIAN_POINT('Ctrl Pts',(-26.6919359630255,24.2685535091901,-60.4774158315639));
#13250=CARTESIAN_POINT('Ctrl Pts',(-26.6927532925958,24.2649692902955,-60.477188389835));
#13251=CARTESIAN_POINT('Ctrl Pts',(-26.6965384370844,24.2482383535136,-60.4761287485988));
#13252=CARTESIAN_POINT('Ctrl Pts',(-26.6994299538781,24.2350742490567,-60.4753008959832));
#13253=CARTESIAN_POINT('Ctrl Pts',(-26.74906901666,24.002119477145,-60.4607486871998));
#13254=CARTESIAN_POINT('Ctrl Pts',(-26.7727935821034,23.7780118663693,-60.4482581935681));
#13255=CARTESIAN_POINT('Ctrl Pts',(-26.7732463754423,23.2876823900882,-60.4208610712342));
#13256=CARTESIAN_POINT('Ctrl Pts',(-26.7406739381063,23.0231686516336,-60.4059680650802));
#13257=CARTESIAN_POINT('Ctrl Pts',(-26.6719080673939,22.7492082193554,-60.3888514686056));
#13258=CARTESIAN_POINT('Ctrl Pts',(-26.6676488242134,22.7327896199245,-60.3878194777504));
#13259=CARTESIAN_POINT('Ctrl Pts',(-26.6617572843645,22.7107946837967,-60.3864284225943));
#13260=CARTESIAN_POINT('Ctrl Pts',(-26.6602391777089,22.7051878210366,-60.3860730707556));
#13261=CARTESIAN_POINT('Ctrl Pts',(-26.6578368700494,22.6964094649833,-60.385515530349));
#13262=CARTESIAN_POINT('Ctrl Pts',(-26.6569629481102,22.6932351509118,-60.385313676611));
#13263=CARTESIAN_POINT('Ctrl Pts',(-26.6552781358949,22.6871519123201,-60.3849263763411));
#13264=CARTESIAN_POINT('Ctrl Pts',(-26.6544680178596,22.6842427758264,-60.3847409551444));
#13265=CARTESIAN_POINT('Ctrl Pts',(-26.6525586641544,22.6774233837778,-60.3843058190168));
#13266=CARTESIAN_POINT('Ctrl Pts',(-26.6514561243334,22.673514065722,-60.3840559965292));
#13267=CARTESIAN_POINT('Ctrl Pts',(-26.6482588983541,22.6622590283134,-60.3833356661077));
#13268=CARTESIAN_POINT('Ctrl Pts',(-26.6461454933531,22.6549186954897,-60.3828645474292));
#13269=CARTESIAN_POINT('Ctrl Pts',(-26.6318564287939,22.6059450804685,-60.3797123224051));
#13270=CARTESIAN_POINT('Ctrl Pts',(-26.6188678717204,22.5645554487225,-60.3770046973106));
#13271=CARTESIAN_POINT('Ctrl Pts',(-26.5794712779629,22.4473492411775,-60.3692076783081));
#13272=CARTESIAN_POINT('Ctrl Pts',(-26.5510619272762,22.372244444364,-60.364053818291));
#13273=CARTESIAN_POINT('Ctrl Pts',(-26.4061930513277,22.0286204290436,-60.3397305670125));
#13274=CARTESIAN_POINT('Ctrl Pts',(-26.2563305119106,21.7757494827836,-60.3195089192671));
#13275=CARTESIAN_POINT('Ctrl Pts',(-26.0587389409155,21.5268271426935,-60.29843339558));
#13276=CARTESIAN_POINT('Ctrl Pts',(-26.0428177301035,21.5072466184985,-60.2967679691044));
#13277=CARTESIAN_POINT('Ctrl Pts',(-26.0077540878592,21.4651441020893,-60.2931736371484));
#13278=CARTESIAN_POINT('Ctrl Pts',(-25.9885281964672,21.4426940005698,-60.291248570365));
#13279=CARTESIAN_POINT('Ctrl Pts',(-25.9679114778802,21.4192796380399,-60.289234526886));
#13280=CARTESIAN_POINT('Ctrl Pts',(-25.9668264535615,21.4180492736216,-60.2891286755375));
#13281=CARTESIAN_POINT('Ctrl Pts',(-25.9639429072803,21.4147845017821,-60.2888477509164));
#13282=CARTESIAN_POINT('Ctrl Pts',(-25.9621427487103,21.4127515335335,-60.2886727699528));
#13283=CARTESIAN_POINT('Ctrl Pts',(-25.9342793988578,21.3813647067349,-60.2859705175049));
#13284=CARTESIAN_POINT('Ctrl Pts',(-25.9076830965851,21.3524854876379,-60.2834741706482));
#13285=CARTESIAN_POINT('Ctrl Pts',(-25.8772690046277,21.3206483840594,-60.2807180082568));
#13286=CARTESIAN_POINT('Ctrl Pts',(-25.8739660214299,21.3172061956836,-60.2804199603599));
#13287=CARTESIAN_POINT('Ctrl Pts',(-25.8689829863096,21.3120361773187,-60.2799722401627));
#13288=CARTESIAN_POINT('Ctrl Pts',(-25.8673086381527,21.3103028961506,-60.2798221280879));
#13289=CARTESIAN_POINT('Ctrl Pts',(-25.8644065981706,21.3073054470718,-60.2795625153158));
#13290=CARTESIAN_POINT('Ctrl Pts',(-25.863179813925,21.3060404082637,-60.2794529436332));
#13291=CARTESIAN_POINT('Ctrl Pts',(-25.8606227285272,21.3034079096273,-60.2792249196519));
#13292=CARTESIAN_POINT('Ctrl Pts',(-25.8592922521642,21.302040626327,-60.27910648204));
#13293=CARTESIAN_POINT('Ctrl Pts',(-25.8561298682358,21.2987965250996,-60.2788254552662));
#13294=CARTESIAN_POINT('Ctrl Pts',(-25.8542968769134,21.2969207549273,-60.2786629514398));
#13295=CARTESIAN_POINT('Ctrl Pts',(-25.8481798467253,21.2906762315511,-60.2781219219332));
#13296=CARTESIAN_POINT('Ctrl Pts',(-25.843885622343,21.2863174071223,-60.2777441938289));
#13297=CARTESIAN_POINT('Ctrl Pts',(-25.7339332116331,21.1753448781149,-60.2681247002332));
#13298=CARTESIAN_POINT('Ctrl Pts',(-25.6209505014655,21.0762130932694,-60.2594621356334));
#13299=CARTESIAN_POINT('Ctrl Pts',(-25.2266298362415,20.7762462886088,-60.2314428530723));
#13300=CARTESIAN_POINT('Ctrl Pts',(-24.9200302400552,20.6127269577628,-60.2127350488086));
#13301=CARTESIAN_POINT('Ctrl Pts',(-24.5736710963128,20.4942480773045,-60.1906023336608));
#13302=CARTESIAN_POINT('Ctrl Pts',(-24.5539588339682,20.4877172402958,-60.1893406636643));
#13303=CARTESIAN_POINT('Ctrl Pts',(-24.5281870217807,20.4794543664092,-60.1876880630845));
#13304=CARTESIAN_POINT('Ctrl Pts',(-24.5221832673577,20.4775488552878,-60.187302858969));
#13305=CARTESIAN_POINT('Ctrl Pts',(-24.512938777715,20.4746445830253,-60.1867093804247));
#13306=CARTESIAN_POINT('Ctrl Pts',(-24.5097019644707,20.473633307936,-60.1865015178778));
#13307=CARTESIAN_POINT('Ctrl Pts',(-24.5035129025046,20.4717103807978,-60.1861039397958));
#13308=CARTESIAN_POINT('Ctrl Pts',(-24.5005609254372,20.4707978614519,-60.1859142530105));
#13309=CARTESIAN_POINT('Ctrl Pts',(-24.4939821344908,20.4687745767321,-60.1854913910076));
#13310=CARTESIAN_POINT('Ctrl Pts',(-24.4903546667502,20.4676659675275,-60.1852581453017));
#13311=CARTESIAN_POINT('Ctrl Pts',(-24.4828235028081,20.4653788593902,-60.1847737135551));
#13312=CARTESIAN_POINT('Ctrl Pts',(-24.4789195122102,20.4642013608137,-60.1845224951607));
#13313=CARTESIAN_POINT('Ctrl Pts',(-24.4690467269631,20.4612440202674,-60.1838869334775));
#13314=CARTESIAN_POINT('Ctrl Pts',(-24.4630750074428,20.4594740724996,-60.1835022666312));
#13315=CARTESIAN_POINT('Ctrl Pts',(-24.4460792567874,20.4544902831809,-60.182406797972));
#13316=CARTESIAN_POINT('Ctrl Pts',(-24.4350432117285,20.4513180587282,-60.1816946385476));
#13317=CARTESIAN_POINT('Ctrl Pts',(-24.3320864241747,20.4223187421607,-60.1750427702001));
#13318=CARTESIAN_POINT('Ctrl Pts',(-24.2390861345507,20.4005320373902,-60.1689724382176));
#13319=CARTESIAN_POINT('Ctrl Pts',(-24.004007049572,20.3563705808468,-60.1534586637642));
#13320=CARTESIAN_POINT('Ctrl Pts',(-23.861148132463,20.3393163339329,-60.1438726191102));
#13321=CARTESIAN_POINT('Ctrl Pts',(-23.4685052022661,20.3188949414558,-60.1173428601809));
#13322=CARTESIAN_POINT('Ctrl Pts',(-23.218688492532,20.3349080054325,-60.1002178852915));
#13323=CARTESIAN_POINT('Ctrl Pts',(-22.9715167725327,20.379892073931,-60.0843396011012));
#13324=CARTESIAN_POINT('Ctrl Pts',(-22.9698276212348,20.3802008863058,-60.0842311444443));
#13325=CARTESIAN_POINT('Ctrl Pts',(-22.9551315079401,20.3828997848357,-60.0832880163971));
#13326=CARTESIAN_POINT('Ctrl Pts',(-22.9421388600796,20.3853686107999,-60.0824574589776));
#13327=CARTESIAN_POINT('Ctrl Pts',(-22.9255800102334,20.3886208128835,-60.0814034046504));
#13328=CARTESIAN_POINT('Ctrl Pts',(-22.9219996836921,20.389330317569,-60.0811757661517));
#13329=CARTESIAN_POINT('Ctrl Pts',(-22.9163120632797,20.3904674648851,-60.0808145785833));
#13330=CARTESIAN_POINT('Ctrl Pts',(-22.9142039923915,20.3908911339368,-60.0806808020035));
#13331=CARTESIAN_POINT('Ctrl Pts',(-22.9102665642947,20.3916865582267,-60.0804311147867));
#13332=CARTESIAN_POINT('Ctrl Pts',(-22.9084371183133,20.3920577906453,-60.0803151751567));
#13333=CARTESIAN_POINT('Ctrl Pts',(-22.9043333061843,20.3928942521003,-60.0800552612188));
#13334=CARTESIAN_POINT('Ctrl Pts',(-22.9020591245228,20.3933603481401,-60.0799113377675));
#13335=CARTESIAN_POINT('Ctrl Pts',(-22.8953375682649,20.3947455079494,-60.0794862823139));
#13336=CARTESIAN_POINT('Ctrl Pts',(-22.8908916067557,20.3956715202934,-60.0792055493185));
#13337=CARTESIAN_POINT('Ctrl Pts',(-22.8561511833587,20.4029839668509,-60.0770150948339));
#13338=CARTESIAN_POINT('Ctrl Pts',(-22.8259468834668,20.4097975326101,-60.0751295237575));
#13339=CARTESIAN_POINT('Ctrl Pts',(-22.721399238305,20.4349703426456,-60.0686538158082));
#13340=CARTESIAN_POINT('Ctrl Pts',(-22.6476107524568,20.4555440508272,-60.0641730975848));
#13341=CARTESIAN_POINT('Ctrl Pts',(-22.2005956387554,20.5975330376361,-60.0371952096772));
#13342=CARTESIAN_POINT('Ctrl Pts',(-21.8514278405479,20.7836368432619,-60.0163814734318));
#13343=CARTESIAN_POINT('Ctrl Pts',(-21.5291801313123,21.039923026942,-59.9914650763811));
#13344=CARTESIAN_POINT('Ctrl Pts',(-21.514227017287,21.0520355776059,-59.9902952741229));
#13345=CARTESIAN_POINT('Ctrl Pts',(-21.4946683069979,21.0681710619137,-59.9887467403859));
#13346=CARTESIAN_POINT('Ctrl Pts',(-21.4899641924846,21.0720743932321,-59.9883728771842));
#13347=CARTESIAN_POINT('Ctrl Pts',(-21.4826965269162,21.0781398772748,-59.9877930552217));
#13348=CARTESIAN_POINT('Ctrl Pts',(-21.4801251802715,21.0802927025087,-59.9875874782779));
#13349=CARTESIAN_POINT('Ctrl Pts',(-21.4750465664753,21.0845582046866,-59.9871805891671));
#13350=CARTESIAN_POINT('Ctrl Pts',(-21.472539153398,21.086670702357,-59.9869792844975));
#13351=CARTESIAN_POINT('Ctrl Pts',(-21.4669882325931,21.0913618600593,-59.9865327110262));
#13352=CARTESIAN_POINT('Ctrl Pts',(-21.4639462837389,21.093942348823,-59.9862873670885));
#13353=CARTESIAN_POINT('Ctrl Pts',(-21.4576440747357,21.099308672978,-59.9857777830139));
#13354=CARTESIAN_POINT('Ctrl Pts',(-21.454384570063,21.1020953799092,-59.9855135071006));
#13355=CARTESIAN_POINT('Ctrl Pts',(-21.4460255395166,21.1092708450883,-59.9848339133412));
#13356=CARTESIAN_POINT('Ctrl Pts',(-21.4409341962258,21.1136690655456,-59.9844182031825));
#13357=CARTESIAN_POINT('Ctrl Pts',(-21.4262184822622,21.126462107367,-59.9832114592914));
#13358=CARTESIAN_POINT('Ctrl Pts',(-21.4166302760253,21.1348981629209,-59.9824187070848));
#13359=CARTESIAN_POINT('Ctrl Pts',(-21.3219449984661,21.2192094884072,-59.9745249400231));
#13360=CARTESIAN_POINT('Ctrl Pts',(-21.2408904697627,21.2994842673907,-59.9672369285417));
#13361=CARTESIAN_POINT('Ctrl Pts',(-20.9518788759671,21.6177936213176,-59.9391271575394));
#13362=CARTESIAN_POINT('Ctrl Pts',(-20.7750808025658,21.8816243356112,-59.9171542691619));
#13363=CARTESIAN_POINT('Ctrl Pts',(-20.6339599973371,22.1785668680963,-59.8956329389504));
#13364=CARTESIAN_POINT('Ctrl Pts',(-20.6284970787806,22.1902419477057,-59.894791883197));
#13365=CARTESIAN_POINT('Ctrl Pts',(-20.6217678309579,22.2048510584192,-59.8937460948862));
#13366=CARTESIAN_POINT('Ctrl Pts',(-20.6204356954141,22.2077544599115,-59.8935385813245));
#13367=CARTESIAN_POINT('Ctrl Pts',(-20.5974696451716,22.2580061642565,-59.8899526460202));
#13368=CARTESIAN_POINT('Ctrl Pts',(-20.5769801645026,22.305873305525,-59.886623986611));
#13369=CARTESIAN_POINT('Ctrl Pts',(-20.5555330361776,22.3595361541265,-59.8830045854945));
#13370=CARTESIAN_POINT('Ctrl Pts',(-20.5534221766376,22.3648588532698,-59.8826467975053));
#13371=CARTESIAN_POINT('Ctrl Pts',(-20.5504841832215,22.3723252431736,-59.8821466380858));
#13372=CARTESIAN_POINT('Ctrl Pts',(-20.5496451549772,22.3744641951248,-59.8820035518201));
#13373=CARTESIAN_POINT('Ctrl Pts',(-20.5481137853683,22.3783804616915,-59.8817419360491));
#13374=CARTESIAN_POINT('Ctrl Pts',(-20.5474207334757,22.3801574961055,-59.8816233633248));
#13375=CARTESIAN_POINT('Ctrl Pts',(-20.5460158306932,22.3837692357584,-59.8813826502418));
#13376=CARTESIAN_POINT('Ctrl Pts',(-20.5453040825019,22.3856039782304,-59.8812605162119));
#13377=CARTESIAN_POINT('Ctrl Pts',(-20.5435389010194,22.3901666482865,-59.8809571532225));
#13378=CARTESIAN_POINT('Ctrl Pts',(-20.5424874964873,22.392895366893,-59.8807760475502));
#13379=CARTESIAN_POINT('Ctrl Pts',(-20.5385674895896,22.4031104117441,-59.8800992614596));
#13380=CARTESIAN_POINT('Ctrl Pts',(-20.5357230802018,22.4106060840939,-59.8796050310142));
#13381=CARTESIAN_POINT('Ctrl Pts',(-20.4870559471141,22.5403122648878,-59.8710926994827));
#13382=CARTESIAN_POINT('Ctrl Pts',(-20.448664598178,22.6652021184694,-59.8635059766248));
#13383=CARTESIAN_POINT('Ctrl Pts',(-20.3325695051864,23.144843102361,-59.8354431374785));
#13384=CARTESIAN_POINT('Ctrl Pts',(-20.3073857211801,23.5094492477192,-59.8159319005925));
#13385=CARTESIAN_POINT('Ctrl Pts',(-20.3454822205398,23.8908067036625,-59.7927534642006));
#13386=CARTESIAN_POINT('Ctrl Pts',(-20.3476915544303,23.9109921176318,-59.7915195411324));
#13387=CARTESIAN_POINT('Ctrl Pts',(-20.3508294299338,23.9373550559754,-59.7898983061721));
#13388=CARTESIAN_POINT('Ctrl Pts',(-20.3515854162371,23.9435529664887,-59.7895164541467));
#13389=CARTESIAN_POINT('Ctrl Pts',(-20.3527783977376,23.9531025655446,-59.788927012087));
#13390=CARTESIAN_POINT('Ctrl Pts',(-20.3532026652215,23.9564558530042,-59.7887198249462));
#13391=CARTESIAN_POINT('Ctrl Pts',(-20.3540485785778,23.9630582817905,-59.7883114734609));
#13392=CARTESIAN_POINT('Ctrl Pts',(-20.3544699055831,23.9663074604516,-59.7881103194403));
#13393=CARTESIAN_POINT('Ctrl Pts',(-20.3554090288439,23.9734641711262,-59.7876668175839));
#13394=CARTESIAN_POINT('Ctrl Pts',(-20.3559290401142,23.9773714031831,-59.7874243998415));
#13395=CARTESIAN_POINT('Ctrl Pts',(-20.3570216128152,23.9854671137423,-59.7869215175256));
#13396=CARTESIAN_POINT('Ctrl Pts',(-20.3575952496855,23.9896554368692,-59.7866610192838));
#13397=CARTESIAN_POINT('Ctrl Pts',(-20.3590833003289,24.0003634535025,-59.7859941662426));
#13398=CARTESIAN_POINT('Ctrl Pts',(-20.3600094509001,24.0068814724731,-59.7855874396385));
#13399=CARTESIAN_POINT('Ctrl Pts',(-20.3627369434881,24.025663499535,-59.7844130758635));
#13400=CARTESIAN_POINT('Ctrl Pts',(-20.3645890631126,24.0379199095502,-59.783643829848));
#13401=CARTESIAN_POINT('Ctrl Pts',(-20.3833396521092,24.157334795555,-59.7761202414873));
#13402=CARTESIAN_POINT('Ctrl Pts',(-20.4055660477846,24.2635746653563,-59.7691968112395));
#13403=CARTESIAN_POINT('Ctrl Pts',(-20.5076589473408,24.6525102416091,-59.742967301939));
#13404=CARTESIAN_POINT('Ctrl Pts',(-20.620665503439,24.9249619521829,-59.7226710832638));
#13405=CARTESIAN_POINT('Ctrl Pts',(-20.7855596407207,25.206654778394,-59.7010354244668));
#13406=CARTESIAN_POINT('Ctrl Pts',(-20.8025757232645,25.2347309308273,-59.6988732390526));
#13407=CARTESIAN_POINT('Ctrl Pts',(-20.8233731137638,25.2678922118154,-59.696316606057));
#13408=CARTESIAN_POINT('Ctrl Pts',(-20.826743629861,25.2732315488106,-59.6959048714288));
#13409=CARTESIAN_POINT('Ctrl Pts',(-20.8325007101426,25.2822924110081,-59.6952060502973));
#13410=CARTESIAN_POINT('Ctrl Pts',(-20.8348792683038,25.2860189756452,-59.6949186072461));
#13411=CARTESIAN_POINT('Ctrl Pts',(-20.8658609259485,25.3343394179612,-59.6911911942636));
#13412=CARTESIAN_POINT('Ctrl Pts',(-20.8955538891357,25.3782296230703,-59.687802258331));
#13413=CARTESIAN_POINT('Ctrl Pts',(-20.9296574274634,25.4260542139122,-59.6841233180694));
#13414=CARTESIAN_POINT('Ctrl Pts',(-20.9330097520276,25.4307287705315,-59.6837638745796));
#13415=CARTESIAN_POINT('Ctrl Pts',(-20.9377211259396,25.437261412281,-59.6832617958988));
#13416=CARTESIAN_POINT('Ctrl Pts',(-20.9390696518484,25.4391270191997,-59.683118438574));
#13417=CARTESIAN_POINT('Ctrl Pts',(-20.9415398818594,25.4425367375025,-59.6828564810674));
#13418=CARTESIAN_POINT('Ctrl Pts',(-20.9426609602028,25.4440812993772,-59.6827378372621));
#13419=CARTESIAN_POINT('Ctrl Pts',(-20.9449399348785,25.4472152889306,-59.6824971451542));
#13420=CARTESIAN_POINT('Ctrl Pts',(-20.9460979142873,25.4488046532217,-59.6823751029067));
#13421=CARTESIAN_POINT('Ctrl Pts',(-20.9489773693219,25.4527492077706,-59.6820722645127));
#13422=CARTESIAN_POINT('Ctrl Pts',(-20.9507005938854,25.4551031283689,-59.6818915907353));
#13423=CARTESIAN_POINT('Ctrl Pts',(-20.9571427979019,25.4638781403062,-59.6812182269761));
#13424=CARTESIAN_POINT('Ctrl Pts',(-20.9618824422396,25.4702841315971,-59.6807269679622));
#13425=CARTESIAN_POINT('Ctrl Pts',(-21.042738075588,25.5787231797695,-59.6724151693296));
#13426=CARTESIAN_POINT('Ctrl Pts',(-21.1248205688843,25.6761900693949,-59.6650049607331));
#13427=CARTESIAN_POINT('Ctrl Pts',(-21.2396954761958,25.7972524485473,-59.6555032889791));
#13428=CARTESIAN_POINT('Ctrl Pts',(-21.2674520610817,25.8254458558071,-59.6532675425095));
#13429=CARTESIAN_POINT('Ctrl Pts',(-21.3194355529443,25.8763382036649,-59.6491738555093));
#13430=CARTESIAN_POINT('Ctrl Pts',(-21.3435073542389,25.8991873340857,-59.6473133430677));
#13431=CARTESIAN_POINT('Ctrl Pts',(-21.519366350419,26.0610242549589,-59.6339376814138));
#13432=CARTESIAN_POINT('Ctrl Pts',(-21.6837944063406,26.185551545305,-59.6225339060881));
#13433=CARTESIAN_POINT('Ctrl Pts',(-21.9294086191048,26.3369764848424,-59.6057496661577));
#13434=CARTESIAN_POINT('Ctrl Pts',(-22.0014847055492,26.377668243201,-59.6008566094396));
#13435=CARTESIAN_POINT('Ctrl Pts',(-22.075036024144,26.4155367790859,-59.5958634867516));
#13436=CARTESIAN_POINT('Origin',(-23.5502525316942,23.5502525316942,-77.3107734492734));
#13437=CARTESIAN_POINT('',(-22.0750360153446,26.4155367745555,-58.0990855609687));
#13438=CARTESIAN_POINT('',(-22.0750360184326,26.4155367761454,-58.3433576442193));
#13439=CARTESIAN_POINT('',(-22.0750360153461,26.4155367745563,-77.3107734492734));
#13440=CARTESIAN_POINT('',(-26.7730012761155,23.5474077415013,-58.9401251418819));
#13441=CARTESIAN_POINT('Ctrl Pts',(-22.0750360153447,26.4155367745556,-58.0990855609687));
#13442=CARTESIAN_POINT('Ctrl Pts',(-22.0676980781123,26.4117587737418,-58.0996197687782));
#13443=CARTESIAN_POINT('Ctrl Pts',(-22.0603745949641,26.40795255408,-58.1001526872996));
#13444=CARTESIAN_POINT('Ctrl Pts',(-22.0472928179374,26.4010896298236,-58.101104098468));
#13445=CARTESIAN_POINT('Ctrl Pts',(-22.04152905953,26.3980435259965,-58.1015231000164));
#13446=CARTESIAN_POINT('Ctrl Pts',(-22.006154855784,26.3792109822164,-58.1040933420527));
#13447=CARTESIAN_POINT('Ctrl Pts',(-21.9767817886019,26.362979605031,-58.1062218758795));
#13448=CARTESIAN_POINT('Ctrl Pts',(-21.9432746360227,26.3437745428648,-58.1086387338298));
#13449=CARTESIAN_POINT('Ctrl Pts',(-21.9388889696207,26.3412470955953,-58.1089548455282));
#13450=CARTESIAN_POINT('Ctrl Pts',(-21.9324322481283,26.33750581313,-58.1094198828372));
#13451=CARTESIAN_POINT('Ctrl Pts',(-21.930356592747,26.3362999957308,-58.1095693254527));
#13452=CARTESIAN_POINT('Ctrl Pts',(-21.9266585544373,26.3341461522102,-58.1098354772508));
#13453=CARTESIAN_POINT('Ctrl Pts',(-21.9250356534901,26.3331990263661,-58.1099522451026));
#13454=CARTESIAN_POINT('Ctrl Pts',(-21.9216212244718,26.3312023584053,-58.1101978408928));
#13455=CARTESIAN_POINT('Ctrl Pts',(-21.9198298863959,26.3301525067484,-58.1103266478328));
#13456=CARTESIAN_POINT('Ctrl Pts',(-21.9151539504061,26.3274060008881,-58.1106627670032));
#13457=CARTESIAN_POINT('Ctrl Pts',(-21.9122709689688,26.3257065778639,-58.1108698981324));
#13458=CARTESIAN_POINT('Ctrl Pts',(-21.8994961879407,26.3181494257741,-58.1117872725112));
#13459=CARTESIAN_POINT('Ctrl Pts',(-21.8896329652453,26.3122431883853,-58.1124943801649));
#13460=CARTESIAN_POINT('Ctrl Pts',(-21.8164728214048,26.267900284789,-58.1177321208777));
#13461=CARTESIAN_POINT('Ctrl Pts',(-21.7544802898064,26.2273415121784,-58.1221301319267));
#13462=CARTESIAN_POINT('Ctrl Pts',(-21.5146177149416,26.0583252013949,-58.1392138911113));
#13463=CARTESIAN_POINT('Ctrl Pts',(-21.3486559233651,25.9139839060101,-58.1512192756305));
#13464=CARTESIAN_POINT('Ctrl Pts',(-21.0584009032197,25.6042376117704,-58.1750957309266));
#13465=CARTESIAN_POINT('Ctrl Pts',(-20.9327933122848,25.4415661769213,-58.1868752194558));
#13466=CARTESIAN_POINT('Ctrl Pts',(-20.8167823733491,25.2574189671903,-58.2001006083787));
#13467=CARTESIAN_POINT('Ctrl Pts',(-20.8101283603662,25.2467182294559,-58.2008686025562));
#13468=CARTESIAN_POINT('Ctrl Pts',(-20.801120909131,25.2320415274055,-58.2019213317536));
#13469=CARTESIAN_POINT('Ctrl Pts',(-20.7987129497811,25.2280990184376,-58.2022040587783));
#13470=CARTESIAN_POINT('Ctrl Pts',(-20.7946284692472,25.2213791317761,-58.2026858605033));
#13471=CARTESIAN_POINT('Ctrl Pts',(-20.7929476443894,25.2186043667002,-58.202884776991));
#13472=CARTESIAN_POINT('Ctrl Pts',(-20.7897042251249,25.2132317258738,-58.2032698765809));
#13473=CARTESIAN_POINT('Ctrl Pts',(-20.7881411007254,25.2106341733627,-58.2034560399559));
#13474=CARTESIAN_POINT('Ctrl Pts',(-20.7844398409519,25.2044638418469,-58.2038982058074));
#13475=CARTESIAN_POINT('Ctrl Pts',(-20.7823049636181,25.2008891237492,-58.2041543270289));
#13476=CARTESIAN_POINT('Ctrl Pts',(-20.7760254800232,25.1903280832651,-58.2049108835963));
#13477=CARTESIAN_POINT('Ctrl Pts',(-20.77190037682,25.1833302550905,-58.2054120289657));
#13478=CARTESIAN_POINT('Ctrl Pts',(-20.7404896447349,25.1295815763913,-58.2092601410414));
#13479=CARTESIAN_POINT('Ctrl Pts',(-20.7143607465427,25.0821679730332,-58.2126487448131));
#13480=CARTESIAN_POINT('Ctrl Pts',(-20.6301858525942,24.9198836275427,-58.2242371249276));
#13481=CARTESIAN_POINT('Ctrl Pts',(-20.57783495408,24.8022132150835,-58.2326293352103));
#13482=CARTESIAN_POINT('Ctrl Pts',(-20.4561958696138,24.4778112538357,-58.2556765888785));
#13483=CARTESIAN_POINT('Ctrl Pts',(-20.4006035785347,24.2666709324352,-58.2706171881914));
#13484=CARTESIAN_POINT('Ctrl Pts',(-20.3600662468127,24.0092337271706,-58.287988379156));
#13485=CARTESIAN_POINT('Ctrl Pts',(-20.3542475297845,23.9667913336922,-58.2908235599343));
#13486=CARTESIAN_POINT('Ctrl Pts',(-20.3483768832184,23.9165447411626,-58.2941373910606));
#13487=CARTESIAN_POINT('Ctrl Pts',(-20.3475050957034,23.9088421499098,-58.2946442052975));
#13488=CARTESIAN_POINT('Ctrl Pts',(-20.3461382922348,23.8963631505231,-58.2954633079041));
#13489=CARTESIAN_POINT('Ctrl Pts',(-20.3456261496483,23.8915886885315,-58.2957762252108));
#13490=CARTESIAN_POINT('Ctrl Pts',(-20.3443979737639,23.8798925440261,-58.2965416071583));
#13491=CARTESIAN_POINT('Ctrl Pts',(-20.3436936805637,23.8729696216578,-58.2969936226092));
#13492=CARTESIAN_POINT('Ctrl Pts',(-20.3427377752082,23.863261270265,-58.2976260387367));
#13493=CARTESIAN_POINT('Ctrl Pts',(-20.3424673624957,23.8604777593476,-58.2978071917035));
#13494=CARTESIAN_POINT('Ctrl Pts',(-20.3420714545763,23.8563465872066,-58.2980757973916));
#13495=CARTESIAN_POINT('Ctrl Pts',(-20.3419431852754,23.8549992004073,-58.2981633633647));
#13496=CARTESIAN_POINT('Ctrl Pts',(-20.341574694818,23.8511024256803,-58.2984164960507));
#13497=CARTESIAN_POINT('Ctrl Pts',(-20.3413366627182,23.8485528258432,-58.2985819724549));
#13498=CARTESIAN_POINT('Ctrl Pts',(-20.3408755492314,23.8435493407495,-58.2989064263341));
#13499=CARTESIAN_POINT('Ctrl Pts',(-20.3406522428451,23.8410954784192,-58.2990654131508));
#13500=CARTESIAN_POINT('Ctrl Pts',(-20.3400483178405,23.8343736817508,-58.2995005464906));
#13501=CARTESIAN_POINT('Ctrl Pts',(-20.3396733949605,23.8301052246053,-58.2997764499088));
#13502=CARTESIAN_POINT('Ctrl Pts',(-20.3361143381287,23.7886370720046,-58.3024527592119));
#13503=CARTESIAN_POINT('Ctrl Pts',(-20.3335681853829,23.7513834179954,-58.3048250615296));
#13504=CARTESIAN_POINT('Ctrl Pts',(-20.3314043717874,23.7088758725424,-58.3074891336274));
#13505=CARTESIAN_POINT('Ctrl Pts',(-20.3311515279812,23.7036590817678,-58.3078153509713));
#13506=CARTESIAN_POINT('Ctrl Pts',(-20.3307995631067,23.6960128053208,-58.3082923906593));
#13507=CARTESIAN_POINT('Ctrl Pts',(-20.3306905092495,23.6935838194159,-58.3084437689834));
#13508=CARTESIAN_POINT('Ctrl Pts',(-20.330501858767,23.6892730839687,-58.3087121298965));
#13509=CARTESIAN_POINT('Ctrl Pts',(-20.3304211627993,23.687391387325,-58.3088291747182));
#13510=CARTESIAN_POINT('Ctrl Pts',(-20.3302556427603,23.6834510411808,-58.3090740639089));
#13511=CARTESIAN_POINT('Ctrl Pts',(-20.3301711435147,23.6813923854026,-58.3092018894841));
#13512=CARTESIAN_POINT('Ctrl Pts',(-20.3299573703595,23.6760594238809,-58.3095327197153));
#13513=CARTESIAN_POINT('Ctrl Pts',(-20.3298311155833,23.6727849891043,-58.3097355536263));
#13514=CARTESIAN_POINT('Ctrl Pts',(-20.329309485935,23.6586984447924,-58.310606890668));
#13515=CARTESIAN_POINT('Ctrl Pts',(-20.3289635592016,23.6478844100164,-58.3112726362608));
#13516=CARTESIAN_POINT('Ctrl Pts',(-20.3282038789085,23.6196941266448,-58.3130003393996));
#13517=CARTESIAN_POINT('Ctrl Pts',(-20.3278762164518,23.6023156584231,-58.3140577169823));
#13518=CARTESIAN_POINT('Ctrl Pts',(-20.3272050082794,23.5399494679859,-58.3178274197463));
#13519=CARTESIAN_POINT('Ctrl Pts',(-20.3276628502538,23.4949563344509,-58.3205005251716));
#13520=CARTESIAN_POINT('Ctrl Pts',(-20.332294622686,23.3461559316025,-58.3292301464952));
#13521=CARTESIAN_POINT('Ctrl Pts',(-20.3405450553807,23.2425359462845,-58.3351316956454));
#13522=CARTESIAN_POINT('Ctrl Pts',(-20.3714627845804,23.001941411725,-58.3487726139861));
#13523=CARTESIAN_POINT('Ctrl Pts',(-20.3979980828437,22.865678559511,-58.3564551792907));
#13524=CARTESIAN_POINT('Ctrl Pts',(-20.4825214360355,22.5438756933861,-58.3752117936975));
#13525=CARTESIAN_POINT('Ctrl Pts',(-20.5486544218391,22.3610678807753,-58.3863955534678));
#13526=CARTESIAN_POINT('Ctrl Pts',(-20.6362185896086,22.1737764310991,-58.3989576945894));
#13527=CARTESIAN_POINT('Ctrl Pts',(-20.6416894765885,22.1622535337556,-58.39973507416));
#13528=CARTESIAN_POINT('Ctrl Pts',(-20.6492450379007,22.1465806875915,-58.4007986944732));
#13529=CARTESIAN_POINT('Ctrl Pts',(-20.6512705393168,22.1424022085144,-58.4010828730705));
#13530=CARTESIAN_POINT('Ctrl Pts',(-20.654729326737,22.1353060665916,-58.4015665271959));
#13531=CARTESIAN_POINT('Ctrl Pts',(-20.6561580137894,22.1323861589814,-58.4017658419087));
#13532=CARTESIAN_POINT('Ctrl Pts',(-20.6589267730689,22.1267490723088,-58.4021512182125));
#13533=CARTESIAN_POINT('Ctrl Pts',(-20.6602662641806,22.124031610919,-58.4023372592822));
#13534=CARTESIAN_POINT('Ctrl Pts',(-20.66344901368,22.1175975762233,-58.4027783683807));
#13535=CARTESIAN_POINT('Ctrl Pts',(-20.6652956171162,22.1138826720039,-58.4030335534906));
#13536=CARTESIAN_POINT('Ctrl Pts',(-20.6707467194409,22.1029693356135,-58.4037846815615));
#13537=CARTESIAN_POINT('Ctrl Pts',(-20.6743710042744,22.0957808713245,-58.4042813192077));
#13538=CARTESIAN_POINT('Ctrl Pts',(-20.6996140922977,22.0461765598818,-58.4077215127817));
#13539=CARTESIAN_POINT('Ctrl Pts',(-20.7221425473017,22.0042326206689,-58.4106970834189));
#13540=CARTESIAN_POINT('Ctrl Pts',(-20.775831885522,21.9093756831314,-58.4175855363224));
#13541=CARTESIAN_POINT('Ctrl Pts',(-20.8075917411919,21.8568247261467,-58.4215189577978));
#13542=CARTESIAN_POINT('Ctrl Pts',(-20.9135434584392,21.6923194320745,-58.4342133596874));
#13543=CARTESIAN_POINT('Ctrl Pts',(-20.9932336035815,21.5840892799823,-58.4431546216494));
#13544=CARTESIAN_POINT('Ctrl Pts',(-21.1681837518019,21.3751721726073,-58.4615191270353));
#13545=CARTESIAN_POINT('Ctrl Pts',(-21.2636604968993,21.2750111636965,-58.4709299819139));
#13546=CARTESIAN_POINT('Ctrl Pts',(-21.4401562561203,21.1122227985673,-58.4870230539101));
#13547=CARTESIAN_POINT('Ctrl Pts',(-21.5182793250062,21.0467381821703,-58.4937608064249));
#13548=CARTESIAN_POINT('Ctrl Pts',(-21.6027894829175,20.982466796878,-58.5005570706663));
#13549=CARTESIAN_POINT('Ctrl Pts',(-21.6062037529446,20.9798809140966,-58.5008308375155));
#13550=CARTESIAN_POINT('Ctrl Pts',(-21.6136169374247,20.9742895736466,-58.5014234847939));
#13551=CARTESIAN_POINT('Ctrl Pts',(-21.6176177243386,20.9712865977674,-58.5017422189163));
#13552=CARTESIAN_POINT('Ctrl Pts',(-21.6290213321349,20.9627685303072,-58.5026475321209));
#13553=CARTESIAN_POINT('Ctrl Pts',(-21.6364409511792,20.9572758602866,-58.5032327547009));
#13554=CARTESIAN_POINT('Ctrl Pts',(-21.6553298711226,20.9434178244581,-58.5047127695208));
#13555=CARTESIAN_POINT('Ctrl Pts',(-21.6668311854552,20.9350961060332,-58.5056047909122));
#13556=CARTESIAN_POINT('Ctrl Pts',(-21.681438736159,20.9246732410709,-58.5067258244309));
#13557=CARTESIAN_POINT('Ctrl Pts',(-21.6844939250301,20.922501319016,-58.5069596367153));
#13558=CARTESIAN_POINT('Ctrl Pts',(-21.6893262740061,20.9190786970072,-58.5073284142693));
#13559=CARTESIAN_POINT('Ctrl Pts',(-21.6911009094257,20.917824464229,-58.5074636234271));
#13560=CARTESIAN_POINT('Ctrl Pts',(-21.6944007243967,20.9154973041331,-58.5077146233263));
#13561=CARTESIAN_POINT('Ctrl Pts',(-21.6959255570916,20.9144239122459,-58.5078304459346));
#13562=CARTESIAN_POINT('Ctrl Pts',(-21.6989170597974,20.9123219522417,-58.5080573533617));
#13563=CARTESIAN_POINT('Ctrl Pts',(-21.7003836490148,20.9112932882716,-58.5081684447912));
#13564=CARTESIAN_POINT('Ctrl Pts',(-21.7048382904648,20.9081743461661,-58.5085054221353));
#13565=CARTESIAN_POINT('Ctrl Pts',(-21.7078290467045,20.9060879070071,-58.5087310431794));
#13566=CARTESIAN_POINT('Ctrl Pts',(-21.7228591893839,20.8956403208729,-58.509861841953));
#13567=CARTESIAN_POINT('Ctrl Pts',(-21.734952231348,20.8873561281092,-58.5107618060829));
#13568=CARTESIAN_POINT('Ctrl Pts',(-21.7686038749483,20.8646392561058,-58.5132402317756));
#13569=CARTESIAN_POINT('Ctrl Pts',(-21.790281356902,20.8503836161156,-58.5148075813584));
#13570=CARTESIAN_POINT('Ctrl Pts',(-21.866371494191,20.8016508351184,-58.5202170375516));
#13571=CARTESIAN_POINT('Ctrl Pts',(-21.9216465968004,20.7685425477515,-58.5239850713193));
#13572=CARTESIAN_POINT('Ctrl Pts',(-22.0928426543215,20.6728545290839,-58.5352870652575));
#13573=CARTESIAN_POINT('Ctrl Pts',(-22.2116421700585,20.6157016403082,-58.542636751523));
#13574=CARTESIAN_POINT('Ctrl Pts',(-22.5807721450828,20.4652133067877,-58.5649100679342));
#13575=CARTESIAN_POINT('Ctrl Pts',(-22.8394504606907,20.3955586653664,-58.5798716557515));
#13576=CARTESIAN_POINT('Ctrl Pts',(-23.1205755740448,20.3562293165899,-58.5970729240216));
#13577=CARTESIAN_POINT('Ctrl Pts',(-23.1374304327121,20.3540071587807,-58.5981072514337));
#13578=CARTESIAN_POINT('Ctrl Pts',(-23.1600717566819,20.3512041845243,-58.599500978182));
#13579=CARTESIAN_POINT('Ctrl Pts',(-23.1658435691969,20.3505054926971,-58.5998566467346));
#13580=CARTESIAN_POINT('Ctrl Pts',(-23.1748877487756,20.3494354971894,-58.600414560685));
#13581=CARTESIAN_POINT('Ctrl Pts',(-23.1781588680212,20.3490535822447,-58.6006164704585));
#13582=CARTESIAN_POINT('Ctrl Pts',(-23.1844301651334,20.3483311279619,-58.6010038025725));
#13583=CARTESIAN_POINT('Ctrl Pts',(-23.1874302490794,20.3479897893986,-58.6011891994542));
#13584=CARTESIAN_POINT('Ctrl Pts',(-23.1944648858495,20.3471994267897,-58.6016241655454));
#13585=CARTESIAN_POINT('Ctrl Pts',(-23.1984998094537,20.3467538093702,-58.6018738420661));
#13586=CARTESIAN_POINT('Ctrl Pts',(-23.210119143314,20.3454927858031,-58.602593382873));
#13587=CARTESIAN_POINT('Ctrl Pts',(-23.2177055823441,20.3446966866574,-58.6030638558612));
#13588=CARTESIAN_POINT('Ctrl Pts',(-23.267419499542,20.3396582312481,-58.6061513599894));
#13589=CARTESIAN_POINT('Ctrl Pts',(-23.3096225974221,20.3362196686117,-58.6087936215734));
#13590=CARTESIAN_POINT('Ctrl Pts',(-23.4587829521134,20.3270208203232,-58.6182125562908));
#13591=CARTESIAN_POINT('Ctrl Pts',(-23.5659374406562,20.3257620073106,-58.6251272880969));
#13592=CARTESIAN_POINT('Ctrl Pts',(-23.6991522900978,20.3308373431878,-58.633902722752));
#13593=CARTESIAN_POINT('Ctrl Pts',(-23.7253442638431,20.3321555583475,-58.6356365385109));
#13594=CARTESIAN_POINT('Ctrl Pts',(-23.7725046255801,20.3351065343673,-58.6387727992104));
#13595=CARTESIAN_POINT('Ctrl Pts',(-23.7934788539564,20.3366251869097,-58.6401727725735));
#13596=CARTESIAN_POINT('Ctrl Pts',(-23.9570387609261,20.3500782365292,-58.6511278055667));
#13597=CARTESIAN_POINT('Ctrl Pts',(-24.0986973695205,20.3712910980207,-58.660850623457));
#13598=CARTESIAN_POINT('Ctrl Pts',(-24.3555192692361,20.4274303866719,-58.6786080096213));
#13599=CARTESIAN_POINT('Ctrl Pts',(-24.4710600086441,20.4595259552132,-58.6866440828384));
#13600=CARTESIAN_POINT('Ctrl Pts',(-24.6357011675498,20.5153167156157,-58.6979394414853));
#13601=CARTESIAN_POINT('Ctrl Pts',(-24.6864098796684,20.5339333354284,-58.701395535482));
#13602=CARTESIAN_POINT('Ctrl Pts',(-24.7414705177401,20.5557334763497,-58.7051046983956));
#13603=CARTESIAN_POINT('Ctrl Pts',(-24.7463061572741,20.5576616159926,-58.7054300782113));
#13604=CARTESIAN_POINT('Ctrl Pts',(-24.7534742919255,20.5605399533349,-58.7059118292773));
#13605=CARTESIAN_POINT('Ctrl Pts',(-24.7558103491087,20.5614811696675,-58.7060687382457));
#13606=CARTESIAN_POINT('Ctrl Pts',(-24.759805658087,20.563096358301,-58.7063369372708));
#13607=CARTESIAN_POINT('Ctrl Pts',(-24.7614654509351,20.5637689750498,-58.7064483096216));
#13608=CARTESIAN_POINT('Ctrl Pts',(-24.7647003329701,20.565083023476,-58.7066652777558));
#13609=CARTESIAN_POINT('Ctrl Pts',(-24.766275470778,20.5657243166405,-58.7067708813128));
#13610=CARTESIAN_POINT('Ctrl Pts',(-24.7695384939546,20.5670558184248,-58.7069895590906));
#13611=CARTESIAN_POINT('Ctrl Pts',(-24.7712263037112,20.5677462138613,-58.7071026219168));
#13612=CARTESIAN_POINT('Ctrl Pts',(-24.775085860061,20.5693287834828,-58.7073610553661));
#13613=CARTESIAN_POINT('Ctrl Pts',(-24.777257222713,20.5702219004372,-58.7075063686105));
#13614=CARTESIAN_POINT('Ctrl Pts',(-24.7881906839086,20.5747329875335,-58.7082376714012));
#13615=CARTESIAN_POINT('Ctrl Pts',(-24.7969378865331,20.5783872827729,-58.7088214705853));
#13616=CARTESIAN_POINT('Ctrl Pts',(-24.8191569847031,20.5877850594732,-58.7103014699764));
#13617=CARTESIAN_POINT('Ctrl Pts',(-24.8326062486783,20.5935819383182,-58.711194562987));
#13618=CARTESIAN_POINT('Ctrl Pts',(-24.8877179443487,20.6177828820176,-58.7148447422309));
#13619=CARTESIAN_POINT('Ctrl Pts',(-24.929029529535,20.6369783551149,-58.7175585226573));
#13620=CARTESIAN_POINT('Ctrl Pts',(-25.038897050783,20.6908893097572,-58.7247513583352));
#13621=CARTESIAN_POINT('Ctrl Pts',(-25.1066434994506,20.7271922919223,-58.7291607476499));
#13622=CARTESIAN_POINT('Ctrl Pts',(-25.2319526421024,20.8002246596876,-58.7373847292117));
#13623=CARTESIAN_POINT('Ctrl Pts',(-25.2897705148839,20.8364275257609,-58.7412082993718));
#13624=CARTESIAN_POINT('Ctrl Pts',(-25.4331866769271,20.9326958650035,-58.7508689873099));
#13625=CARTESIAN_POINT('Ctrl Pts',(-25.5170895952792,20.9951409065211,-58.7566893904664));
#13626=CARTESIAN_POINT('Ctrl Pts',(-25.7453076317367,21.182905193803,-58.7733616153561));
#13627=CARTESIAN_POINT('Ctrl Pts',(-25.881703842901,21.3171115633809,-58.7843820318429));
#13628=CARTESIAN_POINT('Ctrl Pts',(-26.0135945835897,21.4722190222821,-58.7967538034128));
#13629=CARTESIAN_POINT('Ctrl Pts',(-26.0217257936253,21.4818963633081,-58.7975241651298));
#13630=CARTESIAN_POINT('Ctrl Pts',(-26.0327546130788,21.4951801787201,-58.7985796429386));
#13631=CARTESIAN_POINT('Ctrl Pts',(-26.0357017741019,21.4987455190106,-58.7988627374433));
#13632=CARTESIAN_POINT('Ctrl Pts',(-26.0407038256966,21.5048233713511,-58.7993450079952));
#13633=CARTESIAN_POINT('Ctrl Pts',(-26.0427626216106,21.5073326729309,-58.7995440251724));
#13634=CARTESIAN_POINT('Ctrl Pts',(-26.0467366927721,21.5121913001278,-58.7999291940737));
#13635=CARTESIAN_POINT('Ctrl Pts',(-26.0486524517203,21.5145402264696,-58.8001153258686));
#13636=CARTESIAN_POINT('Ctrl Pts',(-26.0531894916415,21.5201191761655,-58.8005572213258));
#13637=CARTESIAN_POINT('Ctrl Pts',(-26.0558078334393,21.523351573004,-58.8008131033081));
#13638=CARTESIAN_POINT('Ctrl Pts',(-26.0635090216723,21.5328965733922,-58.8015682707832));
#13639=CARTESIAN_POINT('Ctrl Pts',(-26.0685742942707,21.5392232566404,-58.8020682623589));
#13640=CARTESIAN_POINT('Ctrl Pts',(-26.104816758271,21.5848428724473,-58.8056696757559));
#13641=CARTESIAN_POINT('Ctrl Pts',(-26.1350952345941,21.6248379635473,-58.8088067228743));
#13642=CARTESIAN_POINT('Ctrl Pts',(-26.2600789027057,21.7981937864426,-58.8223292056579));
#13643=CARTESIAN_POINT('Ctrl Pts',(-26.3454785408393,21.9379354158334,-58.8330632564305));
#13644=CARTESIAN_POINT('Ctrl Pts',(-26.4452775221216,22.1331929204328,-58.8477620356812));
#13645=CARTESIAN_POINT('Ctrl Pts',(-26.46936457035,22.1835000676783,-58.8515222097568));
#13646=CARTESIAN_POINT('Ctrl Pts',(-26.5033554884374,22.259494666039,-58.8571500331254));
#13647=CARTESIAN_POINT('Ctrl Pts',(-26.5142558110974,22.2847259649098,-58.8590100903821));
#13648=CARTESIAN_POINT('Ctrl Pts',(-26.5366289812747,22.3383890617118,-58.8629456575821));
#13649=CARTESIAN_POINT('Ctrl Pts',(-26.548021619838,22.3668515552862,-58.8650210698213));
#13650=CARTESIAN_POINT('Ctrl Pts',(-26.6116287801908,22.5325785827677,-58.8770249118301));
#13651=CARTESIAN_POINT('Ctrl Pts',(-26.6548230597419,22.6731351767959,-58.8868963484685));
#13652=CARTESIAN_POINT('Ctrl Pts',(-26.6971868107076,22.8542276156384,-58.8988695096886));
#13653=CARTESIAN_POINT('Ctrl Pts',(-26.7053992795376,22.8924566793656,-58.9013555691152));
#13654=CARTESIAN_POINT('Ctrl Pts',(-26.7139186509395,22.9359549293574,-58.9041301722673));
#13655=CARTESIAN_POINT('Ctrl Pts',(-26.7149103661261,22.9410845333713,-58.9044565224561));
#13656=CARTESIAN_POINT('Ctrl Pts',(-26.716352383139,22.9486418690403,-58.9049360537566));
#13657=CARTESIAN_POINT('Ctrl Pts',(-26.7168123697432,22.9510677097144,-58.9050897861985));
#13658=CARTESIAN_POINT('Ctrl Pts',(-26.7176193916301,22.9553506018734,-58.9053608616994));
#13659=CARTESIAN_POINT('Ctrl Pts',(-26.7179675821122,22.9572074314237,-58.9054782713284));
#13660=CARTESIAN_POINT('Ctrl Pts',(-26.7186888667761,22.9610726560823,-58.9057224359218));
#13661=CARTESIAN_POINT('Ctrl Pts',(-26.7190616834882,22.9630810960332,-58.9058491746159));
#13662=CARTESIAN_POINT('Ctrl Pts',(-26.7198134643567,22.9671526631359,-58.9061058346743));
#13663=CARTESIAN_POINT('Ctrl Pts',(-26.7201923243909,22.9692158088345,-58.9062357500021));
#13664=CARTESIAN_POINT('Ctrl Pts',(-26.7211185777745,22.9742877474075,-58.9065547879852));
#13665=CARTESIAN_POINT('Ctrl Pts',(-26.7216637046492,22.9772969599771,-58.9067437815476));
#13666=CARTESIAN_POINT('Ctrl Pts',(-26.7231557075468,22.9856004924997,-58.9072644863017));
#13667=CARTESIAN_POINT('Ctrl Pts',(-26.7240936204068,22.9908964436128,-58.9075956941462));
#13668=CARTESIAN_POINT('Ctrl Pts',(-26.7567804302506,23.1781927329344,-58.9192783373812));
#13669=CARTESIAN_POINT('Ctrl Pts',(-26.7728381517533,23.3626106922982,-58.9297616610296));
#13670=CARTESIAN_POINT('Ctrl Pts',(-26.7730012761155,23.5474077415013,-58.9401251418819));
#13671=CARTESIAN_POINT('Ctrl Pts',(-26.7730012739202,23.5474052557013,-58.9401250024774));
#13672=CARTESIAN_POINT('Ctrl Pts',(-26.7732608683829,23.8412326648132,-58.9566029448737));
#13673=CARTESIAN_POINT('Ctrl Pts',(-26.733340782425,24.1336947857609,-58.9727791402557));
#13674=CARTESIAN_POINT('Ctrl Pts',(-26.6484731159184,24.4377339379656,-58.9917388195041));
#13675=CARTESIAN_POINT('Ctrl Pts',(-26.6423911128418,24.4586979038837,-58.9930565541008));
#13676=CARTESIAN_POINT('Ctrl Pts',(-26.6332165092135,24.4891617042596,-58.9949873212806));
#13677=CARTESIAN_POINT('Ctrl Pts',(-26.6302918717469,24.4987117987337,-58.9955948874375));
#13678=CARTESIAN_POINT('Ctrl Pts',(-26.6249523802974,24.5158621825253,-58.9966901671647));
#13679=CARTESIAN_POINT('Ctrl Pts',(-26.6225536117075,24.5234674250893,-58.9971773508757));
#13680=CARTESIAN_POINT('Ctrl Pts',(-26.6188689100004,24.5350002986675,-58.9979184229626));
#13681=CARTESIAN_POINT('Ctrl Pts',(-26.6176035962834,24.5389345271198,-58.99817163142));
#13682=CARTESIAN_POINT('Ctrl Pts',(-26.6152996793209,24.546051081217,-58.9986303938245));
#13683=CARTESIAN_POINT('Ctrl Pts',(-26.6142636770095,24.5492342480703,-58.9988358616533));
#13684=CARTESIAN_POINT('Ctrl Pts',(-26.6121853678175,24.5555863060551,-58.9992464131048));
#13685=CARTESIAN_POINT('Ctrl Pts',(-26.6111430964525,24.558755204592,-58.9994514953448));
#13686=CARTESIAN_POINT('Ctrl Pts',(-26.6082043844088,24.5676434775839,-59.0000274733912));
#13687=CARTESIAN_POINT('Ctrl Pts',(-26.6062968281407,24.5733591379023,-59.0003987367213));
#13688=CARTESIAN_POINT('Ctrl Pts',(-26.598446092336,24.5966646416276,-59.0019161650385));
#13689=CARTESIAN_POINT('Ctrl Pts',(-26.5923670806594,24.6142080451918,-59.0030668271421));
#13690=CARTESIAN_POINT('Ctrl Pts',(-26.483483282007,24.9198718448998,-59.0232653071219));
#13691=CARTESIAN_POINT('Ctrl Pts',(-26.3403431394454,25.1918993412259,-59.0438085161982));
#13692=CARTESIAN_POINT('Ctrl Pts',(-26.122303960735,25.4932001015231,-59.0689707730406));
#13693=CARTESIAN_POINT('Ctrl Pts',(-26.0818794021036,25.5455869908224,-59.073437456734));
#13694=CARTESIAN_POINT('Ctrl Pts',(-25.984628194895,25.6638988908192,-59.0836888373863));
#13695=CARTESIAN_POINT('Ctrl Pts',(-25.9266828685318,25.7288454450501,-59.0894418763274));
#13696=CARTESIAN_POINT('Ctrl Pts',(-25.8378748648088,25.8206176742615,-59.0976685217115));
#13697=CARTESIAN_POINT('Ctrl Pts',(-25.8090207088124,25.8493263731886,-59.1002569382835));
#13698=CARTESIAN_POINT('Ctrl Pts',(-25.7771506412614,25.8798563927381,-59.1030182282174));
#13699=CARTESIAN_POINT('Ctrl Pts',(-25.774668643435,25.8822264384678,-59.1032326448881));
#13700=CARTESIAN_POINT('Ctrl Pts',(-25.770550540708,25.8861462347791,-59.1035873550384));
#13701=CARTESIAN_POINT('Ctrl Pts',(-25.7689165953662,25.8876982345043,-59.1037278216318));
#13702=CARTESIAN_POINT('Ctrl Pts',(-25.7659787357775,25.8904828986998,-59.1039798920019));
#13703=CARTESIAN_POINT('Ctrl Pts',(-25.7646754195635,25.8917161884343,-59.1040915443794));
#13704=CARTESIAN_POINT('Ctrl Pts',(-25.7621453147452,25.8941063501156,-59.1043079565341));
#13705=CARTESIAN_POINT('Ctrl Pts',(-25.7609186494036,25.8952633465734,-59.1044127259398));
#13706=CARTESIAN_POINT('Ctrl Pts',(-25.758355407902,25.8976772092257,-59.1046313321033));
#13707=CARTESIAN_POINT('Ctrl Pts',(-25.7570186702366,25.8989338933148,-59.1047451546845));
#13708=CARTESIAN_POINT('Ctrl Pts',(-25.7533147896002,25.9024100050524,-59.1050600396994));
#13709=CARTESIAN_POINT('Ctrl Pts',(-25.7509453582762,25.9046270080543,-59.1052609137029));
#13710=CARTESIAN_POINT('Ctrl Pts',(-25.7416149468307,25.9133307913392,-59.106049729626));
#13711=CARTESIAN_POINT('Ctrl Pts',(-25.7346285109584,25.9197903942894,-59.1066355956259));
#13712=CARTESIAN_POINT('Ctrl Pts',(-25.6074104340123,26.036374389873,-59.1172196381788));
#13713=CARTESIAN_POINT('Ctrl Pts',(-25.479001893401,26.1372667572527,-59.1265506100821));
#13714=CARTESIAN_POINT('Ctrl Pts',(-25.277203368387,26.2724065855713,-59.1402222894373));
#13715=CARTESIAN_POINT('Ctrl Pts',(-25.2092911492622,26.3143207422279,-59.1446712938905));
#13716=CARTESIAN_POINT('Ctrl Pts',(-25.0726217231457,26.3918172543772,-59.1534524638283));
#13717=CARTESIAN_POINT('Ctrl Pts',(-25.0040005429707,26.427528036855,-59.1577811284583));
#13718=CARTESIAN_POINT('Ctrl Pts',(-24.8147219653582,26.5175284127304,-59.1696351132333));
#13719=CARTESIAN_POINT('Ctrl Pts',(-24.6919101877925,26.5669098684925,-59.177240605954));
#13720=CARTESIAN_POINT('Ctrl Pts',(-24.5141753322916,26.6259640425334,-59.1883679519394));
#13721=CARTESIAN_POINT('Ctrl Pts',(-24.4614964891975,26.6419805841453,-59.1916793675401));
#13722=CARTESIAN_POINT('Ctrl Pts',(-24.4005717565787,26.6588118987026,-59.1955329446685));
#13723=CARTESIAN_POINT('Ctrl Pts',(-24.3926997410072,26.6609545135651,-59.1960313082713));
#13724=CARTESIAN_POINT('Ctrl Pts',(-24.3807910055546,26.6641473281262,-59.1967859334832));
#13725=CARTESIAN_POINT('Ctrl Pts',(-24.376760201977,26.6652196311212,-59.1970414764932));
#13726=CARTESIAN_POINT('Ctrl Pts',(-24.369795191123,26.667058041888,-59.1974832550451));
#13727=CARTESIAN_POINT('Ctrl Pts',(-24.3668619562545,26.6678278405865,-59.1976693705194));
#13728=CARTESIAN_POINT('Ctrl Pts',(-24.360791586831,26.6694117945541,-59.198054676264));
#13729=CARTESIAN_POINT('Ctrl Pts',(-24.3576543028627,26.6702253595841,-59.1982538854516));
#13730=CARTESIAN_POINT('Ctrl Pts',(-24.3500531868292,26.6721842593558,-59.1987367220284));
#13731=CARTESIAN_POINT('Ctrl Pts',(-24.345588123993,26.6733247523471,-59.199020506016));
#13732=CARTESIAN_POINT('Ctrl Pts',(-24.3289756402692,26.6775300754888,-59.2000769255727));
#13733=CARTESIAN_POINT('Ctrl Pts',(-24.3168129487212,26.6805336110345,-59.200851541738));
#13734=CARTESIAN_POINT('Ctrl Pts',(-24.120640510273,26.7277658501111,-59.2133649763101));
#13735=CARTESIAN_POINT('Ctrl Pts',(-23.9331381156756,26.7557647998032,-59.2256370411106));
#13736=CARTESIAN_POINT('Ctrl Pts',(-23.6413925320914,26.7733624945439,-59.2451481356751));
#13737=CARTESIAN_POINT('Ctrl Pts',(-23.5382583912424,26.7746282829246,-59.2521176013932));
#13738=CARTESIAN_POINT('Ctrl Pts',(-23.3047978061391,26.7662916668578,-59.2679311097776));
#13739=CARTESIAN_POINT('Ctrl Pts',(-23.1747474262091,26.7537123939401,-59.276767879306));
#13740=CARTESIAN_POINT('Ctrl Pts',(-22.9674149116868,26.7208547603927,-59.2906061974249));
#13741=CARTESIAN_POINT('Ctrl Pts',(-22.8894946101641,26.7055369285702,-59.2957474900287));
#13742=CARTESIAN_POINT('Ctrl Pts',(-22.8039728888793,26.6854169461879,-59.3012668169912));
#13743=CARTESIAN_POINT('Ctrl Pts',(-22.7957408444709,26.6834460030383,-59.3017968049945));
#13744=CARTESIAN_POINT('Ctrl Pts',(-22.7853144837442,26.680906214575,-59.3024663514521));
#13745=CARTESIAN_POINT('Ctrl Pts',(-22.7831129746409,26.6803674815666,-59.3026076280757));
#13746=CARTESIAN_POINT('Ctrl Pts',(-22.7791659036491,26.6793971764419,-59.3028607456617));
#13747=CARTESIAN_POINT('Ctrl Pts',(-22.7774201340876,26.6789664657174,-59.3029726363895));
#13748=CARTESIAN_POINT('Ctrl Pts',(-22.7740362957976,26.6781286108644,-59.303189393757));
#13749=CARTESIAN_POINT('Ctrl Pts',(-22.7723981875171,26.6777216411832,-59.3032942702751));
#13750=CARTESIAN_POINT('Ctrl Pts',(-22.7689868109876,26.6768712767895,-59.3035125611626));
#13751=CARTESIAN_POINT('Ctrl Pts',(-22.767213605066,26.6764276616185,-59.3036259621796));
#13752=CARTESIAN_POINT('Ctrl Pts',(-22.7623266583237,26.6752006416056,-59.303938318523));
#13753=CARTESIAN_POINT('Ctrl Pts',(-22.7592136984493,26.6744140889889,-59.3041370905232));
#13754=CARTESIAN_POINT('Ctrl Pts',(-22.7471078239427,26.6713360397112,-59.3049093379762));
#13755=CARTESIAN_POINT('Ctrl Pts',(-22.738123534142,26.6690103263835,-59.3054808456753));
#13756=CARTESIAN_POINT('Ctrl Pts',(-22.5891559751387,26.6297605476963,-59.3149321045806));
#13757=CARTESIAN_POINT('Ctrl Pts',(-22.4517861027443,26.5834784875011,-59.3232856239594));
#13758=CARTESIAN_POINT('Ctrl Pts',(-22.2354475935959,26.4939548201463,-59.3365297794421));
#13759=CARTESIAN_POINT('Ctrl Pts',(-22.1543980105665,26.4563969913464,-59.341512604251));
#13760=CARTESIAN_POINT('Ctrl Pts',(-22.0750359236218,26.4155367273312,-59.3465003279648));
#13761=CARTESIAN_POINT('',(-26.77300250248,23.5498185963744,-59.1888436164772));
#13762=CARTESIAN_POINT('Ctrl Pts',(-22.075036024144,26.4155367790859,-59.5958634867516));
#13763=CARTESIAN_POINT('Ctrl Pts',(-22.0907483291231,26.4236263959182,-59.5947968373975));
#13764=CARTESIAN_POINT('Ctrl Pts',(-22.1065279599169,26.431587174871,-59.5937256735317));
#13765=CARTESIAN_POINT('Ctrl Pts',(-22.1307918774813,26.443578851968,-59.5920783195984));
#13766=CARTESIAN_POINT('Ctrl Pts',(-22.1392284698494,26.4477025896608,-59.5915054866377));
#13767=CARTESIAN_POINT('Ctrl Pts',(-22.1517665557862,26.4537633566486,-59.590654055701));
#13768=CARTESIAN_POINT('Ctrl Pts',(-22.1558543625232,26.4557287200167,-59.5903764450999));
#13769=CARTESIAN_POINT('Ctrl Pts',(-22.1628524832533,26.4590751535397,-59.5899011542212));
#13770=CARTESIAN_POINT('Ctrl Pts',(-22.1657607523931,26.4604605058275,-59.5897036230776));
#13771=CARTESIAN_POINT('Ctrl Pts',(-22.1716612791766,26.463260371618,-59.5893028329154));
#13772=CARTESIAN_POINT('Ctrl Pts',(-22.1746536475507,26.4646746402418,-59.589099565736));
#13773=CARTESIAN_POINT('Ctrl Pts',(-22.1815163003733,26.4679051788657,-59.5886333654204));
#13774=CARTESIAN_POINT('Ctrl Pts',(-22.1853880247205,26.4697183591702,-59.5883703255992));
#13775=CARTESIAN_POINT('Ctrl Pts',(-22.1935097129092,26.473502167251,-59.5878184975891));
#13776=CARTESIAN_POINT('Ctrl Pts',(-22.1977603855598,26.4754712418729,-59.5875296563324));
#13777=CARTESIAN_POINT('Ctrl Pts',(-22.208983249528,26.4806404117181,-59.586766956327));
#13778=CARTESIAN_POINT('Ctrl Pts',(-22.2159625689602,26.4838248775529,-59.5862925588625));
#13779=CARTESIAN_POINT('Ctrl Pts',(-22.339286178637,26.5395628068426,-59.5779082834818));
#13780=CARTESIAN_POINT('Ctrl Pts',(-22.4586253320777,26.5851756171509,-59.5697605916704));
#13781=CARTESIAN_POINT('Ctrl Pts',(-22.8920280627309,26.7219526713838,-59.5400135355816));
#13782=CARTESIAN_POINT('Ctrl Pts',(-23.2168045732654,26.772318308575,-59.517216217783));
#13783=CARTESIAN_POINT('Ctrl Pts',(-23.5442440032453,26.772997000431,-59.4959384705226));
#13784=CARTESIAN_POINT('Ctrl Pts',(-23.5449153382013,26.7729981821547,-59.4958948538546));
#13785=CARTESIAN_POINT('Ctrl Pts',(-23.552010314682,26.7730084541849,-59.4954339796293));
#13786=CARTESIAN_POINT('Ctrl Pts',(-23.5584340182969,26.7729985487257,-59.495017461577));
#13787=CARTESIAN_POINT('Ctrl Pts',(-23.5660653312186,26.7729639640564,-59.4945235666053));
#13788=CARTESIAN_POINT('Ctrl Pts',(-23.5672729624807,26.772957812332,-59.4944454368121));
#13789=CARTESIAN_POINT('Ctrl Pts',(-23.5714872604604,26.772933975638,-59.4941728822312));
#13790=CARTESIAN_POINT('Ctrl Pts',(-23.5744939151479,26.7729127617385,-59.493978602301));
#13791=CARTESIAN_POINT('Ctrl Pts',(-23.5790754545199,26.7728740239162,-59.4936828246882));
#13792=CARTESIAN_POINT('Ctrl Pts',(-23.5806503552201,26.7728595532461,-59.4935811992677));
#13793=CARTESIAN_POINT('Ctrl Pts',(-23.5848784273599,26.7728176047228,-59.4933084993324));
#13794=CARTESIAN_POINT('Ctrl Pts',(-23.5875315824257,26.7727880047382,-59.4931375146868));
#13795=CARTESIAN_POINT('Ctrl Pts',(-23.6295165929127,26.7722677405198,-59.4904339588933));
#13796=CARTESIAN_POINT('Ctrl Pts',(-23.6688385264976,26.7710602733632,-59.487932429098));
#13797=CARTESIAN_POINT('Ctrl Pts',(-23.7128982078189,26.7688992552242,-59.4851710666132));
#13798=CARTESIAN_POINT('Ctrl Pts',(-23.717665283605,26.7686548244549,-59.4848728450897));
#13799=CARTESIAN_POINT('Ctrl Pts',(-23.7248390033698,26.7682710116682,-59.4844249078419));
#13800=CARTESIAN_POINT('Ctrl Pts',(-23.727246036089,26.7681395205491,-59.4842747517517));
#13801=CARTESIAN_POINT('Ctrl Pts',(-23.7314125650791,26.767907222731,-59.4840150836169));
#13802=CARTESIAN_POINT('Ctrl Pts',(-23.7331721258571,26.7678076734987,-59.4839055005146));
#13803=CARTESIAN_POINT('Ctrl Pts',(-23.7368361167099,26.7675973636017,-59.4836774735867));
#13804=CARTESIAN_POINT('Ctrl Pts',(-23.7387405280093,26.7674863554724,-59.4835590444187));
#13805=CARTESIAN_POINT('Ctrl Pts',(-23.7432621469397,26.7672187617305,-59.4832780736507));
#13806=CARTESIAN_POINT('Ctrl Pts',(-23.7458792718304,26.7670606726053,-59.4831156172941));
#13807=CARTESIAN_POINT('Ctrl Pts',(-23.7545989677662,26.7665232730429,-59.4825749064491));
#13808=CARTESIAN_POINT('Ctrl Pts',(-23.760700699994,26.766129786426,-59.4821974482459));
#13809=CARTESIAN_POINT('Ctrl Pts',(-23.9155571731543,26.7557008222603,-59.472640216683));
#13810=CARTESIAN_POINT('Ctrl Pts',(-24.0634620104508,26.735370359142,-59.4640318816149));
#13811=CARTESIAN_POINT('Ctrl Pts',(-24.2846963989379,26.6891408062855,-59.4512462551058));
#13812=CARTESIAN_POINT('Ctrl Pts',(-24.3593613296593,26.6707285903472,-59.446947851374));
#13813=CARTESIAN_POINT('Ctrl Pts',(-24.5254719582332,26.62340244332,-59.4372960451423));
#13814=CARTESIAN_POINT('Ctrl Pts',(-24.6164275488084,26.593042959063,-59.4319481483246));
#13815=CARTESIAN_POINT('Ctrl Pts',(-24.8785936220146,26.492335802123,-59.4160763611777));
#13816=CARTESIAN_POINT('Ctrl Pts',(-25.0452343999865,26.4112589529476,-59.4053745386004));
#13817=CARTESIAN_POINT('Ctrl Pts',(-25.2139348036433,26.3103998410281,-59.3934227224401));
#13818=CARTESIAN_POINT('Ctrl Pts',(-25.2238495573209,26.3043993799085,-59.3927160774684));
#13819=CARTESIAN_POINT('Ctrl Pts',(-25.2375331703104,26.2960168122115,-59.3917348776431));
#13820=CARTESIAN_POINT('Ctrl Pts',(-25.2413298593136,26.2936801158123,-59.3914619946004));
#13821=CARTESIAN_POINT('Ctrl Pts',(-25.2478438471795,26.2896523804586,-59.3909927078936));
#13822=CARTESIAN_POINT('Ctrl Pts',(-25.2505635056063,26.2879651531547,-59.3907964451272));
#13823=CARTESIAN_POINT('Ctrl Pts',(-25.2560983145071,26.2845200283113,-59.3903963521842));
#13824=CARTESIAN_POINT('Ctrl Pts',(-25.2589132707787,26.2827618283627,-59.3901925109985));
#13825=CARTESIAN_POINT('Ctrl Pts',(-25.265400351582,26.2786961040705,-59.3897219302221));
#13826=CARTESIAN_POINT('Ctrl Pts',(-25.2690705379152,26.2763855132092,-59.3894550770771));
#13827=CARTESIAN_POINT('Ctrl Pts',(-25.2767676395884,26.2715180274725,-59.3888941389022));
#13828=CARTESIAN_POINT('Ctrl Pts',(-25.280793561601,26.2689595883142,-59.3885999967796));
#13829=CARTESIAN_POINT('Ctrl Pts',(-25.2914520282076,26.2621529564421,-59.3878192763049));
#13830=CARTESIAN_POINT('Ctrl Pts',(-25.2980746736699,26.2578893904064,-59.3873321245409));
#13831=CARTESIAN_POINT('Ctrl Pts',(-25.4339852363564,26.1696856731449,-59.3772922012737));
#13832=CARTESIAN_POINT('Ctrl Pts',(-25.5570814497657,26.0766143080507,-59.3673897719349));
#13833=CARTESIAN_POINT('Ctrl Pts',(-25.9307510065266,25.7494942415673,-59.3345840688599));
#13834=CARTESIAN_POINT('Ctrl Pts',(-26.150827876477,25.4842692820876,-59.3105616140563));
#13835=CARTESIAN_POINT('Ctrl Pts',(-26.3262327535223,25.1873405106943,-59.2887641588798));
#13836=CARTESIAN_POINT('Ctrl Pts',(-26.3274426994265,25.1852870925777,-59.2886136516078));
#13837=CARTESIAN_POINT('Ctrl Pts',(-26.3351018861276,25.172255536497,-59.2876599806532));
#13838=CARTESIAN_POINT('Ctrl Pts',(-26.3414884236967,25.1612403909098,-59.2868605721563));
#13839=CARTESIAN_POINT('Ctrl Pts',(-26.3496167888251,25.1470275844363,-59.2858379708155));
#13840=CARTESIAN_POINT('Ctrl Pts',(-26.3514185956687,25.1438646223585,-59.285610959987));
#13841=CARTESIAN_POINT('Ctrl Pts',(-26.3541598209943,25.1390335551401,-59.2852650914879));
#13842=CARTESIAN_POINT('Ctrl Pts',(-26.3551031108158,25.1373676681278,-59.2851459829773));
#13843=CARTESIAN_POINT('Ctrl Pts',(-26.3568699359783,25.1342408905075,-59.2849227180134));
#13844=CARTESIAN_POINT('Ctrl Pts',(-26.3576938123972,25.1327802029616,-59.2848185396237));
#13845=CARTESIAN_POINT('Ctrl Pts',(-26.359583420729,25.1294239117079,-59.2845794412114));
#13846=CARTESIAN_POINT('Ctrl Pts',(-26.3606483724248,25.1275278754472,-59.2844445723346));
#13847=CARTESIAN_POINT('Ctrl Pts',(-26.3635963558023,25.1222668315239,-59.2840709011512));
#13848=CARTESIAN_POINT('Ctrl Pts',(-26.3654752763796,25.1188995059018,-59.2838323649796));
#13849=CARTESIAN_POINT('Ctrl Pts',(-26.3757462915563,25.1004143140987,-59.2825263178782));
#13850=CARTESIAN_POINT('Ctrl Pts',(-26.3840228673712,25.0852320933438,-59.2814661478453));
#13851=CARTESIAN_POINT('Ctrl Pts',(-26.4763747015305,24.912532496034,-59.2695392206124));
#13852=CARTESIAN_POINT('Ctrl Pts',(-26.5473550593576,24.7483314634637,-59.2594338347735));
#13853=CARTESIAN_POINT('Ctrl Pts',(-26.6803649272072,24.3534834145053,-59.2360854118378));
#13854=CARTESIAN_POINT('Ctrl Pts',(-26.7311246740143,24.1201884594064,-59.2229448018575));
#13855=CARTESIAN_POINT('Ctrl Pts',(-26.7630731735512,23.8128200014024,-59.2048042980629));
#13856=CARTESIAN_POINT('Ctrl Pts',(-26.7680772354701,23.7419845696795,-59.2005735311872));
#13857=CARTESIAN_POINT('Ctrl Pts',(-26.77132769563,23.655323377254,-59.1953143184888));
#13858=CARTESIAN_POINT('Ctrl Pts',(-26.7718022479562,23.6395974042291,-59.1943566445975));
#13859=CARTESIAN_POINT('Ctrl Pts',(-26.7722902779298,23.6182381556008,-59.1930512260462));
#13860=CARTESIAN_POINT('Ctrl Pts',(-26.7724041694362,23.6126072106243,-59.1927066356586));
#13861=CARTESIAN_POINT('Ctrl Pts',(-26.7725606275242,23.60371940819,-59.1921620312279));
#13862=CARTESIAN_POINT('Ctrl Pts',(-26.7726130187481,23.6004627167359,-59.1919623258699));
#13863=CARTESIAN_POINT('Ctrl Pts',(-26.7727080303603,23.5939420817654,-59.191562167882));
#13864=CARTESIAN_POINT('Ctrl Pts',(-26.7727506290721,23.5906781416752,-59.1913617148007));
#13865=CARTESIAN_POINT('Ctrl Pts',(-26.7728257346826,23.5841652255821,-59.1909614226252));
#13866=CARTESIAN_POINT('Ctrl Pts',(-26.7728582872022,23.5809162540493,-59.1907615852135));
#13867=CARTESIAN_POINT('Ctrl Pts',(-26.7729314674546,23.5723138260732,-59.1902320641864));
#13868=CARTESIAN_POINT('Ctrl Pts',(-26.7729636687342,23.566960324726,-59.1899021162766));
#13869=CARTESIAN_POINT('Ctrl Pts',(-26.7729963741845,23.5576773933244,-59.1893292634518));
#13870=CARTESIAN_POINT('Ctrl Pts',(-26.7730030315629,23.5537479876886,-59.1890865530728));
#13871=CARTESIAN_POINT('Ctrl Pts',(-26.77300250248,23.5498185963744,-59.1888436164772));
#13872=CARTESIAN_POINT('Ctrl Pts',(-26.7730025025656,23.5498192324511,-59.1888436558029));
#13873=CARTESIAN_POINT('Ctrl Pts',(-26.773001493321,23.5423127732231,-59.18837956523));
#13874=CARTESIAN_POINT('Ctrl Pts',(-26.7729742579153,23.5348063789239,-59.1879146498276));
#13875=CARTESIAN_POINT('Ctrl Pts',(-26.772760049621,23.5047300513712,-59.1860484802711));
#13876=CARTESIAN_POINT('Ctrl Pts',(-26.7723622029,23.4821627072763,-59.1846406279805));
#13877=CARTESIAN_POINT('Ctrl Pts',(-26.7624295140548,23.1291823529402,-59.1624974702859));
#13878=CARTESIAN_POINT('Ctrl Pts',(-26.7023500228878,22.8022180374915,-59.1399985090511));
#13879=CARTESIAN_POINT('Ctrl Pts',(-26.5476562774506,22.3580846319751,-59.1083315251701));
#13880=CARTESIAN_POINT('Ctrl Pts',(-26.4930734416804,22.2290756608938,-59.0990339118501));
#13881=CARTESIAN_POINT('Ctrl Pts',(-26.4232031559689,22.0899374103821,-59.089187054409));
#13882=CARTESIAN_POINT('Ctrl Pts',(-26.4160331239415,22.0759163541898,-59.0881969728356));
#13883=CARTESIAN_POINT('Ctrl Pts',(-26.4070327165654,22.0586297462103,-59.0869795470382));
#13884=CARTESIAN_POINT('Ctrl Pts',(-26.4052992125504,22.0553144027677,-59.0867462095823));
#13885=CARTESIAN_POINT('Ctrl Pts',(-26.4025607549246,22.0500992123996,-59.0863794023107));
#13886=CARTESIAN_POINT('Ctrl Pts',(-26.4015596741883,22.0481973526393,-59.0862456872293));
#13887=CARTESIAN_POINT('Ctrl Pts',(-26.3996854940338,22.0446453981056,-59.0859960555776));
#13888=CARTESIAN_POINT('Ctrl Pts',(-26.398812869228,22.042995071591,-59.0858801101372));
#13889=CARTESIAN_POINT('Ctrl Pts',(-26.3968512641765,22.0392930305608,-59.0856201074755));
#13890=CARTESIAN_POINT('Ctrl Pts',(-26.3957615018503,22.0372417390399,-59.0854761012659));
#13891=CARTESIAN_POINT('Ctrl Pts',(-26.3929873240509,22.032033421415,-59.0851106127568));
#13892=CARTESIAN_POINT('Ctrl Pts',(-26.3912998616306,22.0288780098104,-59.0848893245861));
#13893=CARTESIAN_POINT('Ctrl Pts',(-26.3819864042907,22.0115321670171,-59.0836735983018));
#13894=CARTESIAN_POINT('Ctrl Pts',(-26.3742591681456,21.9973959289755,-59.0826855278183));
#13895=CARTESIAN_POINT('Ctrl Pts',(-26.2206724689657,21.7213622104056,-59.0634331963671));
#13896=CARTESIAN_POINT('Ctrl Pts',(-26.0390554905465,21.4809746675581,-59.0473022214729));
#13897=CARTESIAN_POINT('Ctrl Pts',(-25.7388581089325,21.1813802753183,-59.0233877385789));
#13898=CARTESIAN_POINT('Ctrl Pts',(-25.6459344015434,21.0987910225589,-59.0162864636352));
#13899=CARTESIAN_POINT('Ctrl Pts',(-25.5092062488695,20.9907361952427,-59.0060282902832));
#13900=CARTESIAN_POINT('Ctrl Pts',(-25.4692146261042,20.9606178818691,-59.0030496950771));
#13901=CARTESIAN_POINT('Ctrl Pts',(-25.405567293561,20.9149681303556,-58.9983325178941));
#13902=CARTESIAN_POINT('Ctrl Pts',(-25.3823800687041,20.8987953189399,-58.9966187188258));
#13903=CARTESIAN_POINT('Ctrl Pts',(-25.3549649188277,20.8802049031615,-58.9945968341571));
#13904=CARTESIAN_POINT('Ctrl Pts',(-25.3509400629459,20.8774888771044,-58.9943001089124));
#13905=CARTESIAN_POINT('Ctrl Pts',(-25.3432571038042,20.8723295458039,-58.993733899174));
#13906=CARTESIAN_POINT('Ctrl Pts',(-25.3396001029525,20.8698846123788,-58.9934644769106));
#13907=CARTESIAN_POINT('Ctrl Pts',(-25.333166978255,20.8656026997601,-58.9929906770902));
#13908=CARTESIAN_POINT('Ctrl Pts',(-25.3303929866641,20.8637625160226,-58.9927864206593));
#13909=CARTESIAN_POINT('Ctrl Pts',(-25.3249620015248,20.8601718667398,-58.9923866144038));
#13910=CARTESIAN_POINT('Ctrl Pts',(-25.3223052560885,20.8584210310031,-58.9921910787959));
#13911=CARTESIAN_POINT('Ctrl Pts',(-25.3159789397954,20.8542653166898,-58.9917255633078));
#13912=CARTESIAN_POINT('Ctrl Pts',(-25.3123070488822,20.8518639959391,-58.9914554503136));
#13913=CARTESIAN_POINT('Ctrl Pts',(-25.2992745000029,20.8433789937982,-58.9904970170305));
#13914=CARTESIAN_POINT('Ctrl Pts',(-25.289887228619,20.8373365153003,-58.9898071585941));
#13915=CARTESIAN_POINT('Ctrl Pts',(-25.1554749916149,20.7518013984008,-58.9799358843084));
#13916=CARTESIAN_POINT('Ctrl Pts',(-25.0251640015263,20.6809856074506,-58.9704330579586));
#13917=CARTESIAN_POINT('Ctrl Pts',(-24.7387144853635,20.5499995875361,-58.9496684935595));
#13918=CARTESIAN_POINT('Ctrl Pts',(-24.5818182177269,20.4925043887988,-58.9383638698499));
#13919=CARTESIAN_POINT('Ctrl Pts',(-24.2489790965615,20.3990793709074,-58.9149747778814));
#13920=CARTESIAN_POINT('Ctrl Pts',(-24.0730198135801,20.3651558245771,-58.902934154453));
#13921=CARTESIAN_POINT('Ctrl Pts',(-23.8780520935766,20.3441707699378,-58.8905173615161));
#13922=CARTESIAN_POINT('Ctrl Pts',(-23.8609529428767,20.3424685455815,-58.8894362249869));
#13923=CARTESIAN_POINT('Ctrl Pts',(-23.8400081922989,20.3405525411167,-58.8881222119395));
#13924=CARTESIAN_POINT('Ctrl Pts',(-23.836175186629,20.3402088235604,-58.8878821608513));
#13925=CARTESIAN_POINT('Ctrl Pts',(-23.8301769474359,20.3396817715871,-58.8875071746285));
#13926=CARTESIAN_POINT('Ctrl Pts',(-23.828012144642,20.3394937612997,-58.8873719757501));
#13927=CARTESIAN_POINT('Ctrl Pts',(-23.8241763027714,20.3391645319003,-58.8871326581322));
#13928=CARTESIAN_POINT('Ctrl Pts',(-23.8225053528891,20.3390224284224,-58.8870284896526));
#13929=CARTESIAN_POINT('Ctrl Pts',(-23.818925306572,20.3387207830438,-58.8868054814773));
#13930=CARTESIAN_POINT('Ctrl Pts',(-23.8170161839889,20.3385616395919,-58.886686664888));
#13931=CARTESIAN_POINT('Ctrl Pts',(-23.8114724715318,20.3381044957956,-58.8863419512227));
#13932=CARTESIAN_POINT('Ctrl Pts',(-23.8078375012695,20.3378109609793,-58.886116307049));
#13933=CARTESIAN_POINT('Ctrl Pts',(-23.7914489263278,20.336515529497,-58.8851006611446));
#13934=CARTESIAN_POINT('Ctrl Pts',(-23.7786896927308,20.3355833890863,-58.8843145488998));
#13935=CARTESIAN_POINT('Ctrl Pts',(-23.763630047216,20.3345733050214,-58.8833917900231));
#13936=CARTESIAN_POINT('Ctrl Pts',(-23.7613349261343,20.3344218340624,-58.8832512989139));
#13937=CARTESIAN_POINT('Ctrl Pts',(-23.4171124108492,20.3120742981944,-58.8622010455887));
#13938=CARTESIAN_POINT('Ctrl Pts',(-23.073767506893,20.3445412287019,-58.8440719261785));
#13939=CARTESIAN_POINT('Ctrl Pts',(-22.6057918403408,20.4657929968855,-58.8165083340587));
#13940=CARTESIAN_POINT('Ctrl Pts',(-22.4721205301946,20.509936676184,-58.8083118917589));
#13941=CARTESIAN_POINT('Ctrl Pts',(-22.3214250898988,20.5708931548459,-58.7984876645301));
#13942=CARTESIAN_POINT('Ctrl Pts',(-22.3011657016223,20.5793299086602,-58.7971545189803));
#13943=CARTESIAN_POINT('Ctrl Pts',(-22.2768457398438,20.5897503654097,-58.7955386893125));
#13944=CARTESIAN_POINT('Ctrl Pts',(-22.2727007949349,20.5915366795579,-58.7952627518792));
#13945=CARTESIAN_POINT('Ctrl Pts',(-22.2647503068868,20.5949828604376,-58.794732417683));
#13946=CARTESIAN_POINT('Ctrl Pts',(-22.2609441895033,20.5966413862766,-58.794478067152));
#13947=CARTESIAN_POINT('Ctrl Pts',(-22.254125306114,20.5996284249456,-58.7940215445662));
#13948=CARTESIAN_POINT('Ctrl Pts',(-22.2511113459824,20.6009542111316,-58.7938194662438));
#13949=CARTESIAN_POINT('Ctrl Pts',(-22.2451081529065,20.6036058941484,-58.7934163780103));
#13950=CARTESIAN_POINT('Ctrl Pts',(-22.2421188954367,20.6049317264847,-58.7932153704933));
#13951=CARTESIAN_POINT('Ctrl Pts',(-22.2348260401936,20.6081796360404,-58.792724259124));
#13952=CARTESIAN_POINT('Ctrl Pts',(-22.2305246402726,20.6101066050235,-58.7924339871553));
#13953=CARTESIAN_POINT('Ctrl Pts',(-22.2141782199864,20.6174726792792,-58.7913285468262));
#13954=CARTESIAN_POINT('Ctrl Pts',(-22.2021626000465,20.6229763648518,-58.790511153796));
#13955=CARTESIAN_POINT('Ctrl Pts',(-21.9951387809537,20.7193474001023,-58.7763431402291));
#13956=CARTESIAN_POINT('Ctrl Pts',(-21.8097179649669,20.8294238408003,-58.7622942973665));
#13957=CARTESIAN_POINT('Ctrl Pts',(-21.5123578952181,21.0488584124524,-58.7374755813763));
#13958=CARTESIAN_POINT('Ctrl Pts',(-21.3948043874316,21.1494132456956,-58.7269434856662));
#13959=CARTESIAN_POINT('Ctrl Pts',(-21.1885849452822,21.3532119939397,-58.7074910834349));
#13960=CARTESIAN_POINT('Ctrl Pts',(-21.0983355838537,21.4544056368952,-58.698554858142));
#13961=CARTESIAN_POINT('Ctrl Pts',(-21.011117776681,21.5655746772111,-58.6897042032825));
#13962=CARTESIAN_POINT('Ctrl Pts',(-21.0075348151863,21.5701671533296,-58.6893402108031));
#13963=CARTESIAN_POINT('Ctrl Pts',(-21.0023887198244,21.5768001848321,-58.6888168693726));
#13964=CARTESIAN_POINT('Ctrl Pts',(-21.0008155720644,21.5788329015405,-58.6886568106564));
#13965=CARTESIAN_POINT('Ctrl Pts',(-20.9980845916661,21.5823704281706,-58.6883788224338));
#13966=CARTESIAN_POINT('Ctrl Pts',(-20.9969256555748,21.5838743810739,-58.6882608138101));
#13967=CARTESIAN_POINT('Ctrl Pts',(-20.9946856021041,21.5867866208807,-58.6880326445753));
#13968=CARTESIAN_POINT('Ctrl Pts',(-20.9936043220335,21.5881947734673,-58.6879224721492));
#13969=CARTESIAN_POINT('Ctrl Pts',(-20.9910273633318,21.591556497699,-58.6876598196002));
#13970=CARTESIAN_POINT('Ctrl Pts',(-20.9895327544445,21.5935108935456,-58.6875074159428));
#13971=CARTESIAN_POINT('Ctrl Pts',(-20.9850253884199,21.5994188705874,-58.6870475926769));
#13972=CARTESIAN_POINT('Ctrl Pts',(-20.9820195205409,21.603377735745,-58.686740659253));
#13973=CARTESIAN_POINT('Ctrl Pts',(-20.9516224535746,21.6436049640416,-58.6836336727583));
#13974=CARTESIAN_POINT('Ctrl Pts',(-20.9249905207913,21.6804442200023,-58.6808859070166));
#13975=CARTESIAN_POINT('Ctrl Pts',(-20.8977793166635,21.7198129187281,-58.6780363888251));
#13976=CARTESIAN_POINT('Ctrl Pts',(-20.8964156489309,21.7217905734019,-58.6778934727619));
#13977=CARTESIAN_POINT('Ctrl Pts',(-20.8864714990291,21.7362466036971,-58.6768504450948));
#13978=CARTESIAN_POINT('Ctrl Pts',(-20.877976711757,21.7487840044718,-58.6759547852332));
#13979=CARTESIAN_POINT('Ctrl Pts',(-20.8512017457157,21.7889071608909,-58.6731151766026));
#13980=CARTESIAN_POINT('Ctrl Pts',(-20.8332574976359,21.8167154589597,-58.6711870238619));
#13981=CARTESIAN_POINT('Ctrl Pts',(-20.6703885784722,22.0778575174049,-58.6534002399766));
#13982=CARTESIAN_POINT('Ctrl Pts',(-20.5554178950077,22.3285528735227,-58.6385759778142));
#13983=CARTESIAN_POINT('Ctrl Pts',(-20.4361480242849,22.7110120429233,-58.6156094117335));
#13984=CARTESIAN_POINT('Ctrl Pts',(-20.4057432964606,22.8332954223543,-58.6082348308084));
#13985=CARTESIAN_POINT('Ctrl Pts',(-20.3787897730317,22.9772225194858,-58.5993782083686));
#13986=CARTESIAN_POINT('Ctrl Pts',(-20.3752022182044,22.9974461452436,-58.5981299046236));
#13987=CARTESIAN_POINT('Ctrl Pts',(-20.3710770630506,23.022066501213,-58.5966051590859));
#13988=CARTESIAN_POINT('Ctrl Pts',(-20.3703548347266,23.0264321619743,-58.596334600014));
#13989=CARTESIAN_POINT('Ctrl Pts',(-20.3689827382897,23.0348335049292,-58.5958135562095));
#13990=CARTESIAN_POINT('Ctrl Pts',(-20.3683315522046,23.0388689656509,-58.5955631138558));
#13991=CARTESIAN_POINT('Ctrl Pts',(-20.3671708615304,23.0461499266162,-58.5951109498225));
#13992=CARTESIAN_POINT('Ctrl Pts',(-20.366658637827,23.0493949928832,-58.5949093148692));
#13993=CARTESIAN_POINT('Ctrl Pts',(-20.3655679060968,23.0563743306451,-58.5944754109343));
#13994=CARTESIAN_POINT('Ctrl Pts',(-20.3649910027322,23.0601088446916,-58.5942430912957));
#13995=CARTESIAN_POINT('Ctrl Pts',(-20.363501949916,23.0698617068008,-58.5936359928289));
#13996=CARTESIAN_POINT('Ctrl Pts',(-20.3626002841209,23.0758816189761,-58.5932608817339));
#13997=CARTESIAN_POINT('Ctrl Pts',(-20.3588037268402,23.1017287443471,-58.5916486351362));
#13998=CARTESIAN_POINT('Ctrl Pts',(-20.3560767780575,23.1215798272964,-58.590406186325));
#13999=CARTESIAN_POINT('Ctrl Pts',(-20.304566254436,23.5243818242112,-58.5651060962574));
#14000=CARTESIAN_POINT('Ctrl Pts',(-20.3248178406907,23.912941330978,-58.5385028384232));
#14001=CARTESIAN_POINT('Ctrl Pts',(-20.4317317993905,24.3672543191509,-58.5074053468197));
#14002=CARTESIAN_POINT('Ctrl Pts',(-20.4532261725621,24.4452907280291,-58.5020870212114));
#14003=CARTESIAN_POINT('Ctrl Pts',(-20.4872977750534,24.5529744949696,-58.4948541146297));
#14004=CARTESIAN_POINT('Ctrl Pts',(-20.4974136910194,24.5833635534687,-58.4928250515242));
#14005=CARTESIAN_POINT('Ctrl Pts',(-20.5094920716253,24.6179202466401,-58.4905356654347));
#14006=CARTESIAN_POINT('Ctrl Pts',(-20.5110119627033,24.6222391405069,-58.4902498608063));
#14007=CARTESIAN_POINT('Ctrl Pts',(-20.5133189258569,24.6287502188104,-58.4898194905888));
#14008=CARTESIAN_POINT('Ctrl Pts',(-20.51409917077,24.6309447896521,-58.4896745198874));
#14009=CARTESIAN_POINT('Ctrl Pts',(-20.5155092374294,24.6348972602851,-58.4894135826168));
#14010=CARTESIAN_POINT('Ctrl Pts',(-20.5161382064185,24.6366554544448,-58.4892975653886));
#14011=CARTESIAN_POINT('Ctrl Pts',(-20.517399270915,24.6401709454559,-58.489065703722));
#14012=CARTESIAN_POINT('Ctrl Pts',(-20.5180313632458,24.641928232501,-58.4889498597008));
#14013=CARTESIAN_POINT('Ctrl Pts',(-20.5198210529933,24.6468902227794,-58.4886229121688));
#14014=CARTESIAN_POINT('Ctrl Pts',(-20.5209822102592,24.6500936531925,-58.4884120221826));
#14015=CARTESIAN_POINT('Ctrl Pts',(-20.5258288092757,24.6633986738973,-58.4875368657291));
#14016=CARTESIAN_POINT('Ctrl Pts',(-20.5295597705822,24.6734837800658,-58.486875294705));
#14017=CARTESIAN_POINT('Ctrl Pts',(-20.59806922492,24.8558603580843,-58.4749408711644));
#14018=CARTESIAN_POINT('Ctrl Pts',(-20.6774516131688,25.0223376568686,-58.464511869666));
#14019=CARTESIAN_POINT('Ctrl Pts',(-20.8559396264169,25.3265447913369,-58.444741518809));
#14020=CARTESIAN_POINT('Ctrl Pts',(-20.9525235738024,25.4650210915975,-58.4354088718012));
#14021=CARTESIAN_POINT('Ctrl Pts',(-21.1054726661663,25.6513043714942,-58.4216410975727));
#14022=CARTESIAN_POINT('Ctrl Pts',(-21.1533239035611,25.7057338271597,-58.4174541957901));
#14023=CARTESIAN_POINT('Ctrl Pts',(-21.2395932606114,25.79743489198,-58.4100593058234));
#14024=CARTESIAN_POINT('Ctrl Pts',(-21.2771811350854,25.8354485335515,-58.4068838419896));
#14025=CARTESIAN_POINT('Ctrl Pts',(-21.33709357661,25.893098415411,-58.4018802634256));
#14026=CARTESIAN_POINT('Ctrl Pts',(-21.3587747315375,25.9133911979107,-58.4000808201304));
#14027=CARTESIAN_POINT('Ctrl Pts',(-21.3843724775686,25.9366945237636,-58.3979680376016));
#14028=CARTESIAN_POINT('Ctrl Pts',(-21.3880198559338,25.9399997245624,-58.3976672642202));
#14029=CARTESIAN_POINT('Ctrl Pts',(-21.3949768861788,25.9462751171864,-58.3970940786593));
#14030=CARTESIAN_POINT('Ctrl Pts',(-21.3982851446142,25.9492468424358,-58.3968217320333));
#14031=CARTESIAN_POINT('Ctrl Pts',(-21.4040864974329,25.9544363953292,-58.3963445228957));
#14032=CARTESIAN_POINT('Ctrl Pts',(-21.4065769108486,25.9566572211087,-58.3961397869388));
#14033=CARTESIAN_POINT('Ctrl Pts',(-21.4114387032384,25.9609791872814,-58.3957403342285));
#14034=CARTESIAN_POINT('Ctrl Pts',(-21.4138097413217,25.9630807071136,-58.3955456337144));
#14035=CARTESIAN_POINT('Ctrl Pts',(-21.4194328182804,25.9680498164752,-58.39508414095));
#14036=CARTESIAN_POINT('Ctrl Pts',(-21.4226875469971,25.970914341401,-58.3948172209147));
#14037=CARTESIAN_POINT('Ctrl Pts',(-21.4341147159336,25.9809306766902,-58.3938807691778));
#14038=CARTESIAN_POINT('Ctrl Pts',(-21.4423174471384,25.9880476778286,-58.3932097904491));
#14039=CARTESIAN_POINT('Ctrl Pts',(-21.4560650976963,25.9998543954388,-58.3920872281015));
#14040=CARTESIAN_POINT('Ctrl Pts',(-21.4615902213282,26.0045671104393,-58.391636605378));
#14041=CARTESIAN_POINT('Ctrl Pts',(-21.6537771844614,26.167376127419,-58.3759800759438));
#14042=CARTESIAN_POINT('Ctrl Pts',(-21.8577372505861,26.3036586156245,-58.3598577180973));
#14043=CARTESIAN_POINT('Ctrl Pts',(-22.0750360184326,26.4155367761454,-58.3433576442193));
#14044=CARTESIAN_POINT('Origin',(-23.5502525316942,23.5502525316942,-77.3107734492734));
#14045=CARTESIAN_POINT('',(-22.075035785626,26.4155366562829,-56.8443273945297));
#14046=CARTESIAN_POINT('',(-22.0750360153845,26.415536774576,-57.0898644896988));
#14047=CARTESIAN_POINT('',(-22.0750360153461,26.4155367745563,-77.3107734492734));
#14048=CARTESIAN_POINT('Ctrl Pts',(-22.075035785626,26.4155366562829,-56.8443273945297));
#14049=CARTESIAN_POINT('Ctrl Pts',(-21.9787534219905,26.3659648340796,-56.8514812887004));
#14050=CARTESIAN_POINT('Ctrl Pts',(-21.8849666919604,26.3115384755299,-56.8587625386307));
#14051=CARTESIAN_POINT('Ctrl Pts',(-21.6524805710828,26.1604409150557,-56.8775039548766));
#14052=CARTESIAN_POINT('Ctrl Pts',(-21.5183623236558,26.0574519636375,-56.8890011346993));
#14053=CARTESIAN_POINT('Ctrl Pts',(-21.3414921867163,25.8980789192696,-56.9046470810564));
#14054=CARTESIAN_POINT('Ctrl Pts',(-21.2915601152839,25.8500832300346,-56.9091233591186));
#14055=CARTESIAN_POINT('Ctrl Pts',(-21.2354754770223,25.7925833335758,-56.9141821068135));
#14056=CARTESIAN_POINT('Ctrl Pts',(-21.2277826134483,25.7846145715778,-56.9148766884109));
#14057=CARTESIAN_POINT('Ctrl Pts',(-21.2178451067199,25.7742138879402,-56.9157746549309));
#14058=CARTESIAN_POINT('Ctrl Pts',(-21.2155630338008,25.7718180740115,-56.9159809157184));
#14059=CARTESIAN_POINT('Ctrl Pts',(-21.2118713112045,25.7679303809027,-56.9163146590561));
#14060=CARTESIAN_POINT('Ctrl Pts',(-21.2104593974295,25.7664406699427,-56.9164423181209));
#14061=CARTESIAN_POINT('Ctrl Pts',(-21.207752913517,25.7635795879329,-56.9166870585693));
#14062=CARTESIAN_POINT('Ctrl Pts',(-21.2064581278343,25.7622084334897,-56.9168041566093));
#14063=CARTESIAN_POINT('Ctrl Pts',(-21.2034855259051,25.7590549616847,-56.9170730268537));
#14064=CARTESIAN_POINT('Ctrl Pts',(-21.201808532147,25.7572718644773,-56.9172247347988));
#14065=CARTESIAN_POINT('Ctrl Pts',(-21.1965006081881,25.7516152081032,-56.9177049973031));
#14066=CARTESIAN_POINT('Ctrl Pts',(-21.1928771936804,25.7477345605566,-56.9180329716304));
#14067=CARTESIAN_POINT('Ctrl Pts',(-21.1623460205189,25.7148735016874,-56.9207977646127));
#14068=CARTESIAN_POINT('Ctrl Pts',(-21.1359627199514,25.6854074447381,-56.9231952121615));
#14069=CARTESIAN_POINT('Ctrl Pts',(-21.0144922833713,25.544612351455,-56.9343147534272));
#14070=CARTESIAN_POINT('Ctrl Pts',(-20.9265108846829,25.4273621334583,-56.9426156445672));
#14071=CARTESIAN_POINT('Ctrl Pts',(-20.7540202926931,25.1615422553739,-56.9603937420091));
#14072=CARTESIAN_POINT('Ctrl Pts',(-20.6727316210886,25.0114305752478,-56.9698206861763));
#14073=CARTESIAN_POINT('Ctrl Pts',(-20.5654324896086,24.7692238746175,-56.9849342846938));
#14074=CARTESIAN_POINT('Ctrl Pts',(-20.530987931669,24.6812171312135,-56.9904039706789));
#14075=CARTESIAN_POINT('Ctrl Pts',(-20.4871250515694,24.5527843056446,-56.9984397469981));
#14076=CARTESIAN_POINT('Ctrl Pts',(-20.4745416806035,24.513487937425,-57.0009051438333));
#14077=CARTESIAN_POINT('Ctrl Pts',(-20.4581189076347,24.458594166653,-57.0043631598827));
#14078=CARTESIAN_POINT('Ctrl Pts',(-20.4536360919854,24.4431923313582,-57.0053349057762));
#14079=CARTESIAN_POINT('Ctrl Pts',(-20.4471034785149,24.4201069678507,-57.0067939334481));
#14080=CARTESIAN_POINT('Ctrl Pts',(-20.4449667879056,24.4124481208705,-57.0072783939308));
#14081=CARTESIAN_POINT('Ctrl Pts',(-20.4415854125159,24.4001521470766,-57.0080568631682));
#14082=CARTESIAN_POINT('Ctrl Pts',(-20.4403226996355,24.3955199765698,-57.0083502861289));
#14083=CARTESIAN_POINT('Ctrl Pts',(-20.4379765054927,24.3868367083081,-57.0089006235809));
#14084=CARTESIAN_POINT('Ctrl Pts',(-20.4368905697082,24.3827862794932,-57.0091574578074));
#14085=CARTESIAN_POINT('Ctrl Pts',(-20.4349543714753,24.3755076918735,-57.0096192099041));
#14086=CARTESIAN_POINT('Ctrl Pts',(-20.4341012119435,24.3722803041849,-57.0098240333822));
#14087=CARTESIAN_POINT('Ctrl Pts',(-20.4324488107321,24.3659899530562,-57.0102234008139));
#14088=CARTESIAN_POINT('Ctrl Pts',(-20.431649064064,24.3629271250098,-57.0104179281284));
#14089=CARTESIAN_POINT('Ctrl Pts',(-20.4297672144003,24.3556764301904,-57.010878608629));
#14090=CARTESIAN_POINT('Ctrl Pts',(-20.428689029257,24.3514875606864,-57.0111448885485));
#14091=CARTESIAN_POINT('Ctrl Pts',(-20.4249481560852,24.3368316888835,-57.0120770222557));
#14092=CARTESIAN_POINT('Ctrl Pts',(-20.4223296773429,24.3263535711146,-57.0127443055706));
#14093=CARTESIAN_POINT('Ctrl Pts',(-20.3896846600831,24.1928719732496,-57.0212562561622));
#14094=CARTESIAN_POINT('Ctrl Pts',(-20.3668833237271,24.068231609945,-57.0293339356465));
#14095=CARTESIAN_POINT('Ctrl Pts',(-20.3287378045079,23.7572230138423,-57.0498331318172));
#14096=CARTESIAN_POINT('Ctrl Pts',(-20.3221600858616,23.5702508970748,-57.0624723194976));
#14097=CARTESIAN_POINT('Ctrl Pts',(-20.3412328894607,23.2015053009378,-57.0874566515334));
#14098=CARTESIAN_POINT('Ctrl Pts',(-20.3661302455586,23.0203343057712,-57.0997511017483));
#14099=CARTESIAN_POINT('Ctrl Pts',(-20.4097319132253,22.8267191611916,-57.112304366618));
#14100=CARTESIAN_POINT('Ctrl Pts',(-20.413339323092,22.8112357255337,-57.1133039639425));
#14101=CARTESIAN_POINT('Ctrl Pts',(-20.4179397879531,22.7921308259813,-57.1145315091528));
#14102=CARTESIAN_POINT('Ctrl Pts',(-20.4188247048631,22.7884839244613,-57.1147655689327));
#14103=CARTESIAN_POINT('Ctrl Pts',(-20.4202270348198,22.7827484070829,-57.1151332520048));
#14104=CARTESIAN_POINT('Ctrl Pts',(-20.4207401694365,22.7806587642292,-57.1152671225329));
#14105=CARTESIAN_POINT('Ctrl Pts',(-20.4217023227931,22.7767574530999,-57.115516887477));
#14106=CARTESIAN_POINT('Ctrl Pts',(-20.4221508196027,22.7749456730487,-57.1156328110875));
#14107=CARTESIAN_POINT('Ctrl Pts',(-20.423160111332,22.7708835977116,-57.1158925643706));
#14108=CARTESIAN_POINT('Ctrl Pts',(-20.4237217601743,22.7686335224734,-57.1160363434464));
#14109=CARTESIAN_POINT('Ctrl Pts',(-20.425153358202,22.7629244936862,-57.1164008887338));
#14110=CARTESIAN_POINT('Ctrl Pts',(-20.4260266241675,22.7594663642543,-57.1166214625311));
#14111=CARTESIAN_POINT('Ctrl Pts',(-20.4308409819686,22.7405339818851,-57.1178277569479));
#14112=CARTESIAN_POINT('Ctrl Pts',(-20.4348913906827,22.7250873771118,-57.1188072244354));
#14113=CARTESIAN_POINT('Ctrl Pts',(-20.5147691336677,22.4294404392087,-57.1374745749625));
#14114=CARTESIAN_POINT('Ctrl Pts',(-20.6280092004573,22.1606711405676,-57.1531557945039));
#14115=CARTESIAN_POINT('Ctrl Pts',(-20.8792886873383,21.7354543153442,-57.1809492399011));
#14116=CARTESIAN_POINT('Ctrl Pts',(-20.999180282478,21.570466722419,-57.1926483494376));
#14117=CARTESIAN_POINT('Ctrl Pts',(-21.1393696894901,21.4116006227812,-57.2055271940008));
#14118=CARTESIAN_POINT('Ctrl Pts',(-21.1449499404476,21.4053265402471,-57.2060385987421));
#14119=CARTESIAN_POINT('Ctrl Pts',(-21.1551297342623,21.3939707024617,-57.2069693305155));
#14120=CARTESIAN_POINT('Ctrl Pts',(-21.1597211046626,21.3888816618329,-57.2073883127261));
#14121=CARTESIAN_POINT('Ctrl Pts',(-21.1669304809689,21.3809419164974,-57.2080449634729));
#14122=CARTESIAN_POINT('Ctrl Pts',(-21.1695374657921,21.3780811946546,-57.2082821641948));
#14123=CARTESIAN_POINT('Ctrl Pts',(-21.1742445642324,21.3729346089454,-57.2087099992382));
#14124=CARTESIAN_POINT('Ctrl Pts',(-21.1763428423395,21.3706470662836,-57.2089005552278));
#14125=CARTESIAN_POINT('Ctrl Pts',(-21.1807349368601,21.3658726708806,-57.2092990941281));
#14126=CARTESIAN_POINT('Ctrl Pts',(-21.1830293696387,21.3633863927993,-57.2095071032583));
#14127=CARTESIAN_POINT('Ctrl Pts',(-21.1895805315942,21.3563098567985,-57.2101004886907));
#14128=CARTESIAN_POINT('Ctrl Pts',(-21.1938467091409,21.3517284014341,-57.2104862699737));
#14129=CARTESIAN_POINT('Ctrl Pts',(-21.2121014262799,21.3322388024099,-57.2121343274996));
#14130=CARTESIAN_POINT('Ctrl Pts',(-21.2262180570752,21.3174517737205,-57.2134021250355));
#14131=CARTESIAN_POINT('Ctrl Pts',(-21.4900409326243,21.0463125837041,-57.2369775133577));
#14132=CARTESIAN_POINT('Ctrl Pts',(-21.7805474204764,20.8332339258834,-57.2614182908657));
#14133=CARTESIAN_POINT('Ctrl Pts',(-22.1812457672801,20.6313101870808,-57.2915447075511));
#14134=CARTESIAN_POINT('Ctrl Pts',(-22.2642425301839,20.5938045378977,-57.2975914483371));
#14135=CARTESIAN_POINT('Ctrl Pts',(-22.3939019077899,20.5417077698589,-57.3066372881044));
#14136=CARTESIAN_POINT('Ctrl Pts',(-22.4394908231572,20.524579478675,-57.3097442733959));
#14137=CARTESIAN_POINT('Ctrl Pts',(-22.4901754858377,20.5068368108302,-57.3131045555496));
#14138=CARTESIAN_POINT('Ctrl Pts',(-22.4949014627243,20.5051947793383,-57.3134169845457));
#14139=CARTESIAN_POINT('Ctrl Pts',(-22.5019142418998,20.5027764900608,-57.3138792482548));
#14140=CARTESIAN_POINT('Ctrl Pts',(-22.5041980948744,20.5019917965404,-57.3140295828663));
#14141=CARTESIAN_POINT('Ctrl Pts',(-22.5080928197179,20.5006585270708,-57.3142855911142));
#14142=CARTESIAN_POINT('Ctrl Pts',(-22.5097032441791,20.5001086599058,-57.3143913421599));
#14143=CARTESIAN_POINT('Ctrl Pts',(-22.5130072497662,20.4989834536204,-57.3146080878458));
#14144=CARTESIAN_POINT('Ctrl Pts',(-22.5147008707371,20.4984082500803,-57.3147190742067));
#14145=CARTESIAN_POINT('Ctrl Pts',(-22.5187724384136,20.4970292053672,-57.3149856138111));
#14146=CARTESIAN_POINT('Ctrl Pts',(-22.5211508516008,20.4962267303313,-57.3151410853452));
#14147=CARTESIAN_POINT('Ctrl Pts',(-22.5297992193545,20.4933200267489,-57.315705589506));
#14148=CARTESIAN_POINT('Ctrl Pts',(-22.5360747659316,20.491232302315,-57.3161136467885));
#14149=CARTESIAN_POINT('Ctrl Pts',(-22.6409607842142,20.4566974728741,-57.3229082672942));
#14150=CARTESIAN_POINT('Ctrl Pts',(-22.7410880546166,20.4290104137616,-57.3290203405196));
#14151=CARTESIAN_POINT('Ctrl Pts',(-22.9831577841715,20.3745098512569,-57.3432953426676));
#14152=CARTESIAN_POINT('Ctrl Pts',(-23.1259042470933,20.3523045906114,-57.3513174689769));
#14153=CARTESIAN_POINT('Ctrl Pts',(-23.4180526323383,20.3267718197978,-57.3677092329405));
#14154=CARTESIAN_POINT('Ctrl Pts',(-23.5671537066462,20.3241070382694,-57.3760645612205));
#14155=CARTESIAN_POINT('Ctrl Pts',(-23.8166056746375,20.336945372979,-57.3905342819759));
#14156=CARTESIAN_POINT('Ctrl Pts',(-23.9170076857217,20.3468520829169,-57.3964902163793));
#14157=CARTESIAN_POINT('Ctrl Pts',(-24.0285123938727,20.3631651745485,-57.4033168076524));
#14158=CARTESIAN_POINT('Ctrl Pts',(-24.0402417686993,20.3649473878158,-57.4040375160963));
#14159=CARTESIAN_POINT('Ctrl Pts',(-24.058260471906,20.3677871092181,-57.4051487818947));
#14160=CARTESIAN_POINT('Ctrl Pts',(-24.0645570323616,20.3687986011385,-57.4055378822683));
#14161=CARTESIAN_POINT('Ctrl Pts',(-24.0762592041456,20.3707141090935,-57.4062624817363));
#14162=CARTESIAN_POINT('Ctrl Pts',(-24.0816656007299,20.3716132395239,-57.4065978247122));
#14163=CARTESIAN_POINT('Ctrl Pts',(-24.0905729342214,20.3731179660284,-57.4071512835643));
#14164=CARTESIAN_POINT('Ctrl Pts',(-24.0940752250131,20.373715570819,-57.4073691446976));
#14165=CARTESIAN_POINT('Ctrl Pts',(-24.1009204603798,20.3748952433054,-57.4077954379789));
#14166=CARTESIAN_POINT('Ctrl Pts',(-24.1042634889696,20.3754768017118,-57.4080038536396));
#14167=CARTESIAN_POINT('Ctrl Pts',(-24.1119698175781,20.3768299492102,-57.4084848150498));
#14168=CARTESIAN_POINT('Ctrl Pts',(-24.1163324498675,20.3776052581688,-57.4087574791071));
#14169=CARTESIAN_POINT('Ctrl Pts',(-24.129904648205,20.3800461383003,-57.4096069525183));
#14170=CARTESIAN_POINT('Ctrl Pts',(-24.13910850554,20.3817428201748,-57.4101847536839));
#14171=CARTESIAN_POINT('Ctrl Pts',(-24.2171353188215,20.3964783601849,-57.4150980914831));
#14172=CARTESIAN_POINT('Ctrl Pts',(-24.2855189839271,20.411716857637,-57.419503676993));
#14173=CARTESIAN_POINT('Ctrl Pts',(-24.3607691900882,20.4310797195666,-57.4244684760952));
#14174=CARTESIAN_POINT('Ctrl Pts',(-24.3681836488256,20.4330157791535,-57.4249589249305));
#14175=CARTESIAN_POINT('Ctrl Pts',(-24.4067534386304,20.4432341841526,-57.4275168160622));
#14176=CARTESIAN_POINT('Ctrl Pts',(-24.4377892763695,20.4519569956387,-57.4295975182437));
#14177=CARTESIAN_POINT('Ctrl Pts',(-24.730714678217,20.5390478537564,-57.4494483225039));
#14178=CARTESIAN_POINT('Ctrl Pts',(-24.9817451911856,20.6499708614781,-57.4682160525611));
#14179=CARTESIAN_POINT('Ctrl Pts',(-25.2768349754446,20.8280975517229,-57.4912957714844));
#14180=CARTESIAN_POINT('Ctrl Pts',(-25.3367176130824,20.8670159725454,-57.4960298636663));
#14181=CARTESIAN_POINT('Ctrl Pts',(-25.4214636029922,20.9261892748994,-57.5027541369589));
#14182=CARTESIAN_POINT('Ctrl Pts',(-25.4473933803156,20.9448743219154,-57.5048149752787));
#14183=CARTESIAN_POINT('Ctrl Pts',(-25.4942911135781,20.9797403943836,-57.5085423832999));
#14184=CARTESIAN_POINT('Ctrl Pts',(-25.5153456343185,20.9957999748593,-57.5102158144696));
#14185=CARTESIAN_POINT('Ctrl Pts',(-25.5396381965608,21.0148075431134,-57.512144308288));
#14186=CARTESIAN_POINT('Ctrl Pts',(-25.5430703041788,21.0175042339154,-57.5124167159445));
#14187=CARTESIAN_POINT('Ctrl Pts',(-25.5482903446001,21.0216229267001,-57.5128309358159));
#14188=CARTESIAN_POINT('Ctrl Pts',(-25.5500822441779,21.0230398571851,-57.5129731089533));
#14189=CARTESIAN_POINT('Ctrl Pts',(-25.5531926295689,21.0255047495548,-57.513219861022));
#14190=CARTESIAN_POINT('Ctrl Pts',(-25.5545117973484,21.0265518372424,-57.5133245025078));
#14191=CARTESIAN_POINT('Ctrl Pts',(-25.557273549318,21.0287475054144,-57.5135435534564));
#14192=CARTESIAN_POINT('Ctrl Pts',(-25.5587159644664,21.0298962866376,-57.5136579476473));
#14193=CARTESIAN_POINT('Ctrl Pts',(-25.5627299546159,21.0330987788582,-57.5139762549411));
#14194=CARTESIAN_POINT('Ctrl Pts',(-25.5652993803058,21.0351551993199,-57.5141799726205));
#14195=CARTESIAN_POINT('Ctrl Pts',(-25.5755559084583,21.0433897403,-57.514993039298));
#14196=CARTESIAN_POINT('Ctrl Pts',(-25.5832178887337,21.0495992798684,-57.515600146482));
#14197=CARTESIAN_POINT('Ctrl Pts',(-25.5963664869716,21.0603557432588,-57.5166417442614));
#14198=CARTESIAN_POINT('Ctrl Pts',(-25.6018666928503,21.0648858241562,-57.5170773805794));
#14199=CARTESIAN_POINT('Ctrl Pts',(-25.827318673629,21.2518310391726,-57.534933020719));
#14200=CARTESIAN_POINT('Ctrl Pts',(-26.0220911337097,21.4627069673224,-57.5503992707049));
#14201=CARTESIAN_POINT('Ctrl Pts',(-26.2760799688016,21.8239186922099,-57.5752244890746));
#14202=CARTESIAN_POINT('Ctrl Pts',(-26.3562861527551,21.9576033908593,-57.5841076447431));
#14203=CARTESIAN_POINT('Ctrl Pts',(-26.4529547948706,22.1488698209321,-57.596818849528));
#14204=CARTESIAN_POINT('Ctrl Pts',(-26.4779632331838,22.2018967543072,-57.600341393175));
#14205=CARTESIAN_POINT('Ctrl Pts',(-26.5048224543494,22.2631231298406,-57.6044173391429));
#14206=CARTESIAN_POINT('Ctrl Pts',(-26.5081052950817,22.2706852012635,-57.6049209027706));
#14207=CARTESIAN_POINT('Ctrl Pts',(-26.513012302238,22.2821083562651,-57.6056818241388));
#14208=CARTESIAN_POINT('Ctrl Pts',(-26.5146580327185,22.2859601869963,-57.6059384449492));
#14209=CARTESIAN_POINT('Ctrl Pts',(-26.5174832292158,22.2926084003576,-57.6063814458069));
#14210=CARTESIAN_POINT('Ctrl Pts',(-26.5186662659232,22.2954032675443,-57.6065677038356));
#14211=CARTESIAN_POINT('Ctrl Pts',(-26.5211016763572,22.3011795236997,-57.606952700072));
#14212=CARTESIAN_POINT('Ctrl Pts',(-26.5223535138616,22.3041611340366,-57.6071514562974));
#14213=CARTESIAN_POINT('Ctrl Pts',(-26.5253681444558,22.3113717283107,-57.6076321881781));
#14214=CARTESIAN_POINT('Ctrl Pts',(-26.5271264074449,22.3156025886634,-57.6079143175325));
#14215=CARTESIAN_POINT('Ctrl Pts',(-26.5335933949118,22.3312580484656,-57.6089585022715));
#14216=CARTESIAN_POINT('Ctrl Pts',(-26.5382453754699,22.3427058390163,-57.609722479712));
#14217=CARTESIAN_POINT('Ctrl Pts',(-26.5446068321449,22.3586222317033,-57.6107853453557));
#14218=CARTESIAN_POINT('Ctrl Pts',(-26.5463724105512,22.3630684180858,-57.611082325424));
#14219=CARTESIAN_POINT('Ctrl Pts',(-26.6369540365441,22.592665634321,-57.626421988852));
#14220=CARTESIAN_POINT('Ctrl Pts',(-26.7001152711013,22.8270532248162,-57.6423642392652));
#14221=CARTESIAN_POINT('Ctrl Pts',(-26.7608689148892,23.2269949487658,-57.6696646844548));
#14222=CARTESIAN_POINT('Ctrl Pts',(-26.7730881305036,23.3893607307603,-57.6807487437269));
#14223=CARTESIAN_POINT('Ctrl Pts',(-26.7729839918252,23.5861380660709,-57.6937944397921));
#14224=CARTESIAN_POINT('Ctrl Pts',(-26.7724221417273,23.6203167171048,-57.696045622921));
#14225=CARTESIAN_POINT('Ctrl Pts',(-26.7710409059422,23.6630022442621,-57.6988338138257));
#14226=CARTESIAN_POINT('Ctrl Pts',(-26.7707313581014,23.6715223995904,-57.6993891830459));
#14227=CARTESIAN_POINT('Ctrl Pts',(-26.7682026125359,23.7342620564598,-57.7034697214162));
#14228=CARTESIAN_POINT('Ctrl Pts',(-26.7646479461816,23.7884231079927,-57.7069427870855));
#14229=CARTESIAN_POINT('Ctrl Pts',(-26.7592542071133,23.8476629809551,-57.7106686201622));
#14230=CARTESIAN_POINT('Ctrl Pts',(-26.7587690123611,23.8528524695099,-57.7109943922837));
#14231=CARTESIAN_POINT('Ctrl Pts',(-26.758030548068,23.8605493426267,-57.7114766299617));
#14232=CARTESIAN_POINT('Ctrl Pts',(-26.7577869267436,23.8630576113967,-57.711633634711));
#14233=CARTESIAN_POINT('Ctrl Pts',(-26.7573651013253,23.8673483169139,-57.7119019552955));
#14234=CARTESIAN_POINT('Ctrl Pts',(-26.7571883532734,23.8691308903167,-57.7120133535878));
#14235=CARTESIAN_POINT('Ctrl Pts',(-26.7568409205414,23.8726053798327,-57.7122303363479));
#14236=CARTESIAN_POINT('Ctrl Pts',(-26.7566703834452,23.874297303562,-57.7123359286436));
#14237=CARTESIAN_POINT('Ctrl Pts',(-26.7562552038427,23.8783839431238,-57.7125908093618));
#14238=CARTESIAN_POINT('Ctrl Pts',(-26.7560092167573,23.8807785265179,-57.7127400211164));
#14239=CARTESIAN_POINT('Ctrl Pts',(-26.7552477362043,23.8881104072836,-57.7131964743414));
#14240=CARTESIAN_POINT('Ctrl Pts',(-26.7547235147357,23.8930468208196,-57.7135032227058));
#14241=CARTESIAN_POINT('Ctrl Pts',(-26.7491482654588,23.9444164564389,-57.7166895480072));
#14242=CARTESIAN_POINT('Ctrl Pts',(-26.7430994569822,23.9907388423935,-57.7195136428977));
#14243=CARTESIAN_POINT('Ctrl Pts',(-26.7226699101142,24.1244745162531,-57.7275666461143));
#14244=CARTESIAN_POINT('Ctrl Pts',(-26.7056893718887,24.2114512237485,-57.7326795210357));
#14245=CARTESIAN_POINT('Ctrl Pts',(-26.6020635110297,24.6461158990387,-57.7580858572473));
#14246=CARTESIAN_POINT('Ctrl Pts',(-26.4614706814001,24.9782876357169,-57.7773551319302));
#14247=CARTESIAN_POINT('Ctrl Pts',(-26.2665308637976,25.2846033512845,-57.7992700346422));
#14248=CARTESIAN_POINT('Ctrl Pts',(-26.2639368253878,25.2886593588334,-57.7995609610588));
#14249=CARTESIAN_POINT('Ctrl Pts',(-26.2506227660785,25.3093746453076,-57.801050654163));
#14250=CARTESIAN_POINT('Ctrl Pts',(-26.2397585713089,25.3259403558809,-57.8022546791669));
#14251=CARTESIAN_POINT('Ctrl Pts',(-26.2253040858814,25.3475435423131,-57.8038420411924));
#14252=CARTESIAN_POINT('Ctrl Pts',(-26.2218508843045,25.3526725814879,-57.8042201984081));
#14253=CARTESIAN_POINT('Ctrl Pts',(-26.2164941373886,25.3605797407435,-57.8048051837565));
#14254=CARTESIAN_POINT('Ctrl Pts',(-26.2146009489332,25.3633648876113,-57.805011618792));
#14255=CARTESIAN_POINT('Ctrl Pts',(-26.2108191851299,25.3689096812193,-57.8054233694646));
#14256=CARTESIAN_POINT('Ctrl Pts',(-26.2089306730903,25.371669366255,-57.8056286825275));
#14257=CARTESIAN_POINT('Ctrl Pts',(-26.2047303562659,25.3777868434388,-57.8060846567146));
#14258=CARTESIAN_POINT('Ctrl Pts',(-26.20241647141,25.3811431942882,-57.806335396964));
#14259=CARTESIAN_POINT('Ctrl Pts',(-26.195708654156,25.3908336612321,-57.8070609916497));
#14260=CARTESIAN_POINT('Ctrl Pts',(-26.1912983774939,25.3971563811165,-57.8075364708455));
#14261=CARTESIAN_POINT('Ctrl Pts',(-26.1610596585181,25.4401778253492,-57.8107858762578));
#14262=CARTESIAN_POINT('Ctrl Pts',(-26.1344908947206,25.4763478625879,-57.8135882274604));
#14263=CARTESIAN_POINT('Ctrl Pts',(-26.0696892736973,25.5608118703052,-57.8203061493385));
#14264=CARTESIAN_POINT('Ctrl Pts',(-26.0308112346643,25.6085863363356,-57.8242463799302));
#14265=CARTESIAN_POINT('Ctrl Pts',(-25.9007339311162,25.7593883303221,-57.8371506140417));
#14266=CARTESIAN_POINT('Ctrl Pts',(-25.8043082770192,25.8576904025229,-57.8463078512442));
#14267=CARTESIAN_POINT('Ctrl Pts',(-25.5632799908262,26.0738434254434,-57.8681274292378));
#14268=CARTESIAN_POINT('Ctrl Pts',(-25.4141373371226,26.1859170265834,-57.8808537986894));
#14269=CARTESIAN_POINT('Ctrl Pts',(-25.2422907110606,26.2931326170471,-57.89420728767));
#14270=CARTESIAN_POINT('Ctrl Pts',(-25.2283668889402,26.3016733618467,-57.8952803119659));
#14271=CARTESIAN_POINT('Ctrl Pts',(-25.2022942740452,26.3173945168335,-57.8972721877345));
#14272=CARTESIAN_POINT('Ctrl Pts',(-25.1901621169953,26.324601689438,-57.8981921232258));
#14273=CARTESIAN_POINT('Ctrl Pts',(-25.1323314396259,26.3584444145324,-57.9025430874346));
#14274=CARTESIAN_POINT('Ctrl Pts',(-25.0860258504828,26.3840338305953,-57.9059264710256));
#14275=CARTESIAN_POINT('Ctrl Pts',(-25.0340087644373,26.4111296808668,-57.9095999144229));
#14276=CARTESIAN_POINT('Ctrl Pts',(-25.0289023266027,26.4137722899805,-57.9099591915946));
#14277=CARTESIAN_POINT('Ctrl Pts',(-25.0217420173093,26.4174535279334,-57.9104610726678));
#14278=CARTESIAN_POINT('Ctrl Pts',(-25.0196941030025,26.4185036238587,-57.9106043979786));
#14279=CARTESIAN_POINT('Ctrl Pts',(-25.0159460356058,26.4204204286569,-57.9108663104874));
#14280=CARTESIAN_POINT('Ctrl Pts',(-25.0142462353083,26.4212878223167,-57.9109849412684));
#14281=CARTESIAN_POINT('Ctrl Pts',(-25.0107932636177,26.4230459805743,-57.911225621371));
#14282=CARTESIAN_POINT('Ctrl Pts',(-25.0090400467947,26.4239366506211,-57.9113476646143));
#14283=CARTESIAN_POINT('Ctrl Pts',(-25.0047365582959,26.4261179576918,-57.9116468451782));
#14284=CARTESIAN_POINT('Ctrl Pts',(-25.002185376599,26.4274068108606,-57.9118238691087));
#14285=CARTESIAN_POINT('Ctrl Pts',(-24.9928276937194,26.4321186822439,-57.9124719729086));
#14286=CARTESIAN_POINT('Ctrl Pts',(-24.9860107050494,26.4355209902968,-57.9129417545804));
#14287=CARTESIAN_POINT('Ctrl Pts',(-24.827336825953,26.514012323736,-57.923823335674));
#14288=CARTESIAN_POINT('Ctrl Pts',(-24.6697802347036,26.5770482404036,-57.9335047091121));
#14289=CARTESIAN_POINT('Ctrl Pts',(-24.2514023455975,26.7072626506412,-57.9581501985443));
#14290=CARTESIAN_POINT('Ctrl Pts',(-23.9858723488591,26.7547106949737,-57.9728743723621));
#14291=CARTESIAN_POINT('Ctrl Pts',(-23.6474302666284,26.7723018910867,-57.9928542828013));
#14292=CARTESIAN_POINT('Ctrl Pts',(-23.5772291821286,26.7736539504963,-57.9970562658172));
#14293=CARTESIAN_POINT('Ctrl Pts',(-23.4985063217779,26.7725983841183,-58.0018514492364));
#14294=CARTESIAN_POINT('Ctrl Pts',(-23.4899694716123,26.7724499827105,-58.0023725352038));
#14295=CARTESIAN_POINT('Ctrl Pts',(-23.4771117755208,26.7721753546429,-58.0031590354219));
#14296=CARTESIAN_POINT('Ctrl Pts',(-23.4727903818424,26.7720743551809,-58.0034236578061));
#14297=CARTESIAN_POINT('Ctrl Pts',(-23.4653054452788,26.771884349723,-58.0038824984673));
#14298=CARTESIAN_POINT('Ctrl Pts',(-23.4621417980661,26.771799377068,-58.0040765899116));
#14299=CARTESIAN_POINT('Ctrl Pts',(-23.4555725617038,26.7716132494772,-58.0044799378538));
#14300=CARTESIAN_POINT('Ctrl Pts',(-23.4521669993963,26.771511353802,-58.0046892173429));
#14301=CARTESIAN_POINT('Ctrl Pts',(-23.4441712164299,26.771259425467,-58.0051810008845));
#14302=CARTESIAN_POINT('Ctrl Pts',(-23.4395811511118,26.7711049810236,-58.0054636431608));
#14303=CARTESIAN_POINT('Ctrl Pts',(-23.4246723981896,26.7705714307768,-58.0063827558865));
#14304=CARTESIAN_POINT('Ctrl Pts',(-23.4143552781397,26.7701525478769,-58.007020474494));
#14305=CARTESIAN_POINT('Ctrl Pts',(-23.343413630214,26.7669306976237,-58.0114172380227));
#14306=CARTESIAN_POINT('Ctrl Pts',(-23.2828803141626,26.7624654825156,-58.0152282595712));
#14307=CARTESIAN_POINT('Ctrl Pts',(-23.1248937859085,26.7463151805447,-58.0253397031238));
#14308=CARTESIAN_POINT('Ctrl Pts',(-23.0277907558668,26.7318837341394,-58.0317213407487));
#14309=CARTESIAN_POINT('Ctrl Pts',(-22.6566498980242,26.6592762177837,-58.0567259048995));
#14310=CARTESIAN_POINT('Ctrl Pts',(-22.390007204309,26.5699157114752,-58.0761208336613));
#14311=CARTESIAN_POINT('Ctrl Pts',(-22.1303320224281,26.4433514851374,-58.0950564513809));
#14312=CARTESIAN_POINT('Ctrl Pts',(-22.1223965075359,26.439443246119,-58.095635028738));
#14313=CARTESIAN_POINT('Ctrl Pts',(-22.1100213987141,26.4332850697999,-58.09653705736));
#14314=CARTESIAN_POINT('Ctrl Pts',(-22.1055708048224,26.4310574610118,-58.0968614151201));
#14315=CARTESIAN_POINT('Ctrl Pts',(-22.0952494798854,26.425861503324,-58.0976134880033));
#14316=CARTESIAN_POINT('Ctrl Pts',(-22.0893826209059,26.4228854604864,-58.098040875331));
#14317=CARTESIAN_POINT('Ctrl Pts',(-22.0806931123954,26.4184440855088,-58.0986736844957));
#14318=CARTESIAN_POINT('Ctrl Pts',(-22.0778634908441,26.4169925249115,-58.0988797184485));
#14319=CARTESIAN_POINT('Ctrl Pts',(-22.0750360153447,26.4155367745556,-58.0990855609687));
#14320=CARTESIAN_POINT('Ctrl Pts',(-22.0750360184326,26.4155367761454,-58.3433576442193));
#14321=CARTESIAN_POINT('Ctrl Pts',(-22.0901281593173,26.4233070961395,-58.3422116577876));
#14322=CARTESIAN_POINT('Ctrl Pts',(-22.1052846701242,26.4309597084949,-58.3410642954237));
#14323=CARTESIAN_POINT('Ctrl Pts',(-22.2364279498317,26.4958787601458,-58.3311691557945));
#14324=CARTESIAN_POINT('Ctrl Pts',(-22.3557039933747,26.5462339055725,-58.3223815510167));
#14325=CARTESIAN_POINT('Ctrl Pts',(-22.553438829202,26.6160205043767,-58.3084134789393));
#14326=CARTESIAN_POINT('Ctrl Pts',(-22.6301712337128,26.6399164859788,-58.3031342509527));
#14327=CARTESIAN_POINT('Ctrl Pts',(-22.7384979791312,26.669256976992,-58.2959478750621));
#14328=CARTESIAN_POINT('Ctrl Pts',(-22.7693970680516,26.6771358233143,-58.2939278535823));
#14329=CARTESIAN_POINT('Ctrl Pts',(-22.8048575644904,26.6856193082998,-58.291647585646));
#14330=CARTESIAN_POINT('Ctrl Pts',(-22.8093080065541,26.6866740104269,-58.2913620829709));
#14331=CARTESIAN_POINT('Ctrl Pts',(-22.8160272434295,26.6882512902686,-58.2909320759643));
#14332=CARTESIAN_POINT('Ctrl Pts',(-22.8182943598796,26.6887808838902,-58.2907871675429));
#14333=CARTESIAN_POINT('Ctrl Pts',(-22.8223807979513,26.6897307985846,-58.290526297396));
#14334=CARTESIAN_POINT('Ctrl Pts',(-22.8241999067386,26.6901519942429,-58.2904102851269));
#14335=CARTESIAN_POINT('Ctrl Pts',(-22.8281098736785,26.6910537266933,-58.2901611796793));
#14336=CARTESIAN_POINT('Ctrl Pts',(-22.8302008401002,26.6915337554198,-58.2900281164676));
#14337=CARTESIAN_POINT('Ctrl Pts',(-22.8358302020877,26.6928201869604,-58.2896702877299));
#14338=CARTESIAN_POINT('Ctrl Pts',(-22.8393694963512,26.6936227045079,-58.2894457471868));
#14339=CARTESIAN_POINT('Ctrl Pts',(-22.8556198879532,26.6972785509023,-58.2884167449272));
#14340=CARTESIAN_POINT('Ctrl Pts',(-22.8683470919545,26.7000608211285,-58.2876163319013));
#14341=CARTESIAN_POINT('Ctrl Pts',(-22.8830293897624,26.7031773274554,-58.2866989188954));
#14342=CARTESIAN_POINT('Ctrl Pts',(-22.8849680927801,26.703586973877,-58.286577899838));
#14343=CARTESIAN_POINT('Ctrl Pts',(-23.2228095006068,26.7746471639641,-58.2655095392069));
#14344=CARTESIAN_POINT('Ctrl Pts',(-23.567906180619,26.7911979030126,-58.2473526331973));
#14345=CARTESIAN_POINT('Ctrl Pts',(-24.0484227221739,26.7373483792487,-58.2197786642857));
#14346=CARTESIAN_POINT('Ctrl Pts',(-24.1864965811402,26.7126787446447,-58.2116105343705));
#14347=CARTESIAN_POINT('Ctrl Pts',(-24.3437776431076,26.6738586274887,-58.2018196559438));
#14348=CARTESIAN_POINT('Ctrl Pts',(-24.364984485872,26.6683944383741,-58.2004893077125));
#14349=CARTESIAN_POINT('Ctrl Pts',(-24.3904898875052,26.6615447221525,-58.1988764772228));
#14350=CARTESIAN_POINT('Ctrl Pts',(-24.3948437016583,26.660365658865,-58.1986007122132));
#14351=CARTESIAN_POINT('Ctrl Pts',(-24.4031981011387,26.6580843543161,-58.1980706805382));
#14352=CARTESIAN_POINT('Ctrl Pts',(-24.4071990635825,26.6569835183369,-58.1978164599886));
#14353=CARTESIAN_POINT('Ctrl Pts',(-24.4143697760223,26.6549956426005,-58.1973601375791));
#14354=CARTESIAN_POINT('Ctrl Pts',(-24.4175403196909,26.6541114668468,-58.197158129304));
#14355=CARTESIAN_POINT('Ctrl Pts',(-24.4238586989297,26.6523390109858,-58.1967550696866));
#14356=CARTESIAN_POINT('Ctrl Pts',(-24.4270065481141,26.6514507928497,-58.1965540205635));
#14357=CARTESIAN_POINT('Ctrl Pts',(-24.4346896016542,26.6492702583277,-58.1960627181127));
#14358=CARTESIAN_POINT('Ctrl Pts',(-24.4392233225043,26.6479727794613,-58.1957722963993));
#14359=CARTESIAN_POINT('Ctrl Pts',(-24.4564666728861,26.6429970341364,-58.1946657759572));
#14360=CARTESIAN_POINT('Ctrl Pts',(-24.4691563185353,26.6392505001654,-58.1938474470882));
#14361=CARTESIAN_POINT('Ctrl Pts',(-24.4870642390771,26.6338431935135,-58.1926868165577));
#14362=CARTESIAN_POINT('Ctrl Pts',(-24.4923020262258,26.6322470634876,-58.1923466481552));
#14363=CARTESIAN_POINT('Ctrl Pts',(-24.767995228377,26.5474656083807,-58.174404519575));
#14364=CARTESIAN_POINT('Ctrl Pts',(-25.0262628201694,26.4290552393175,-58.1555401074952));
#14365=CARTESIAN_POINT('Ctrl Pts',(-25.3366535812373,26.2338907704219,-58.1307215842277));
#14366=CARTESIAN_POINT('Ctrl Pts',(-25.4058438380496,26.1865234483561,-58.1250457319403));
#14367=CARTESIAN_POINT('Ctrl Pts',(-25.5774071144353,26.0589679075857,-58.1107107810837));
#14368=CARTESIAN_POINT('Ctrl Pts',(-25.6769326304905,25.9751750381768,-58.1021397977599));
#14369=CARTESIAN_POINT('Ctrl Pts',(-25.7769390418986,25.8800698827541,-58.0934743383474));
#14370=CARTESIAN_POINT('Ctrl Pts',(-25.7827220558217,25.8745290925033,-58.0929730600201));
#14371=CARTESIAN_POINT('Ctrl Pts',(-25.7905875241015,25.8669366337263,-58.0922910942411));
#14372=CARTESIAN_POINT('Ctrl Pts',(-25.7926878675749,25.8649036655304,-58.0921089691174));
#14373=CARTESIAN_POINT('Ctrl Pts',(-25.7961974548516,25.8614973989647,-58.0918046209484));
#14374=CARTESIAN_POINT('Ctrl Pts',(-25.7976082067034,25.8601256676899,-58.0916822751784));
#14375=CARTESIAN_POINT('Ctrl Pts',(-25.8003841359177,25.8574215686437,-58.0914415245286));
#14376=CARTESIAN_POINT('Ctrl Pts',(-25.8017493866195,25.8560892808329,-58.091323113723));
#14377=CARTESIAN_POINT('Ctrl Pts',(-25.804756945263,25.8531491194955,-58.0910622482918));
#14378=CARTESIAN_POINT('Ctrl Pts',(-25.8063987206155,25.8515406968749,-58.0909198369607));
#14379=CARTESIAN_POINT('Ctrl Pts',(-25.8121278365362,25.8459159445214,-58.0904228417465));
#14380=CARTESIAN_POINT('Ctrl Pts',(-25.8162062156746,25.8418904400254,-58.0900689774717));
#14381=CARTESIAN_POINT('Ctrl Pts',(-25.8573352573519,25.8010774741601,-58.0864994064073));
#14382=CARTESIAN_POINT('Ctrl Pts',(-25.89350007992,25.7634030736092,-58.0833526594184));
#14383=CARTESIAN_POINT('Ctrl Pts',(-26.0197251671016,25.6253442577002,-58.0722669413419));
#14384=CARTESIAN_POINT('Ctrl Pts',(-26.1043877662657,25.5202020001471,-58.0646319539541));
#14385=CARTESIAN_POINT('Ctrl Pts',(-26.2802448607012,25.2713314487629,-58.0475402950951));
#14386=CARTESIAN_POINT('Ctrl Pts',(-26.3671461432866,25.1250793680689,-58.0381428572326));
#14387=CARTESIAN_POINT('Ctrl Pts',(-26.4834383916648,24.8886485932731,-58.0231050411599));
#14388=CARTESIAN_POINT('Ctrl Pts',(-26.5210778983742,24.8028808996638,-58.0176822776558));
#14389=CARTESIAN_POINT('Ctrl Pts',(-26.5773391157622,24.6578198157146,-58.0084684836536));
#14390=CARTESIAN_POINT('Ctrl Pts',(-26.5980766828193,24.5994072504514,-58.0047478451513));
#14391=CARTESIAN_POINT('Ctrl Pts',(-26.6196820529002,24.5324896235127,-58.0004613009016));
#14392=CARTESIAN_POINT('Ctrl Pts',(-26.6222167560286,24.52453333954,-57.999951268762));
#14393=CARTESIAN_POINT('Ctrl Pts',(-26.6259830367819,24.5125503819739,-57.9991825135579));
#14394=CARTESIAN_POINT('Ctrl Pts',(-26.6272377046428,24.5085309556233,-57.9989245505107));
#14395=CARTESIAN_POINT('Ctrl Pts',(-26.629384080169,24.5016071974087,-57.9984800128447));
#14396=CARTESIAN_POINT('Ctrl Pts',(-26.630279566999,24.4987040351864,-57.9982935626666));
#14397=CARTESIAN_POINT('Ctrl Pts',(-26.6321172260473,24.4927163084262,-57.9979088998263));
#14398=CARTESIAN_POINT('Ctrl Pts',(-26.6330588755116,24.4896315878501,-57.9977106702276));
#14399=CARTESIAN_POINT('Ctrl Pts',(-26.6353177923541,24.4821916942684,-57.9972324192043));
#14400=CARTESIAN_POINT('Ctrl Pts',(-26.6366304675756,24.4778351435648,-57.9969522475009));
#14401=CARTESIAN_POINT('Ctrl Pts',(-26.6414167832772,24.4618275128665,-57.9959223242517));
#14402=CARTESIAN_POINT('Ctrl Pts',(-26.6448336771732,24.4501596958517,-57.9951707176092));
#14403=CARTESIAN_POINT('Ctrl Pts',(-26.7017644455523,24.2515967720816,-57.982363702013));
#14404=CARTESIAN_POINT('Ctrl Pts',(-26.7383155668851,24.0602919703251,-57.9697439698004));
#14405=CARTESIAN_POINT('Ctrl Pts',(-26.767892425798,23.7607147165483,-57.9496252658992));
#14406=CARTESIAN_POINT('Ctrl Pts',(-26.7730956465111,23.6540869327372,-57.9424040245025));
#14407=CARTESIAN_POINT('Ctrl Pts',(-26.772861301319,23.3891758802995,-57.924472682241));
#14408=CARTESIAN_POINT('Ctrl Pts',(-26.7610689928926,23.2311617293045,-57.9137800574437));
#14409=CARTESIAN_POINT('Ctrl Pts',(-26.7375014584333,23.0732159274586,-57.9034438545549));
#14410=CARTESIAN_POINT('Ctrl Pts',(-26.7372876447135,23.0717895433905,-57.9033505400698));
#14411=CARTESIAN_POINT('Ctrl Pts',(-26.7367475210625,23.0682027218339,-57.903115965739));
#14412=CARTESIAN_POINT('Ctrl Pts',(-26.7364199709727,23.0660424684068,-57.9029747573949));
#14413=CARTESIAN_POINT('Ctrl Pts',(-26.7355283805128,23.0602023414174,-57.902593200423));
#14414=CARTESIAN_POINT('Ctrl Pts',(-26.7349601585361,23.0565230978398,-57.9023530281587));
#14415=CARTESIAN_POINT('Ctrl Pts',(-26.7281319367873,23.0128125434734,-57.8995022225768));
#14416=CARTESIAN_POINT('Ctrl Pts',(-26.7211235438683,22.9728993822419,-57.8969241338947));
#14417=CARTESIAN_POINT('Ctrl Pts',(-26.7123532079817,22.92794655253,-57.8940569634939));
#14418=CARTESIAN_POINT('Ctrl Pts',(-26.7113298090217,22.9227687738263,-57.8937272650322));
#14419=CARTESIAN_POINT('Ctrl Pts',(-26.7098068704688,22.9151619142421,-57.8932437247713));
#14420=CARTESIAN_POINT('Ctrl Pts',(-26.7093172463778,22.9127308923864,-57.8930893185433));
#14421=CARTESIAN_POINT('Ctrl Pts',(-26.7084493118811,22.9084470814102,-57.8928174557374));
#14422=CARTESIAN_POINT('Ctrl Pts',(-26.7080721763578,22.906594058396,-57.8926999313552));
#14423=CARTESIAN_POINT('Ctrl Pts',(-26.7072851619569,22.9027444713818,-57.8924559331465));
#14424=CARTESIAN_POINT('Ctrl Pts',(-26.706875020726,22.9007479678098,-57.8923294749072));
#14425=CARTESIAN_POINT('Ctrl Pts',(-26.7058071045568,22.8955744227002,-57.892002003269));
#14426=CARTESIAN_POINT('Ctrl Pts',(-26.705146423495,22.8923979729896,-57.8918011575165));
#14427=CARTESIAN_POINT('Ctrl Pts',(-26.7023266115158,22.8789427126154,-57.8909512770584));
#14428=CARTESIAN_POINT('Ctrl Pts',(-26.7001220037738,22.8686733404397,-57.890304831939));
#14429=CARTESIAN_POINT('Ctrl Pts',(-26.6606148672541,22.6889299848492,-57.8790259237698));
#14430=CARTESIAN_POINT('Ctrl Pts',(-26.6097280936876,22.5227027977409,-57.8691455014788));
#14431=CARTESIAN_POINT('Ctrl Pts',(-26.470152647353,22.1710390875331,-57.8478980584581));
#14432=CARTESIAN_POINT('Ctrl Pts',(-26.3766508420507,21.9883574811137,-57.8366110561598));
#14433=CARTESIAN_POINT('Ctrl Pts',(-26.2375277905399,21.7704892579177,-57.8217159749355));
#14434=CARTESIAN_POINT('Ctrl Pts',(-26.2074775234427,21.7259278493467,-57.8185889697756));
#14435=CARTESIAN_POINT('Ctrl Pts',(-26.134396636561,21.6231953032932,-57.8111635804617));
#14436=CARTESIAN_POINT('Ctrl Pts',(-26.090495099956,21.565682863672,-57.8068362661166));
#14437=CARTESIAN_POINT('Ctrl Pts',(-26.0386413826668,21.5022950130842,-57.8018485841127));
#14438=CARTESIAN_POINT('Ctrl Pts',(-26.0325515527776,21.4949178537161,-57.8012646589804));
#14439=CARTESIAN_POINT('Ctrl Pts',(-26.0236107877756,21.4841847961321,-57.8004099991146));
#14440=CARTESIAN_POINT('Ctrl Pts',(-26.020785636533,21.4808074059546,-57.8001403183797));
#14441=CARTESIAN_POINT('Ctrl Pts',(-26.0157739019455,21.4748409050574,-57.7996625773101));
#14442=CARTESIAN_POINT('Ctrl Pts',(-26.0135901352503,21.4722494282528,-57.7994546327627));
#14443=CARTESIAN_POINT('Ctrl Pts',(-26.0090536827059,21.4668832181567,-57.7990231153765));
#14444=CARTESIAN_POINT('Ctrl Pts',(-26.0067003790471,21.4641090155697,-57.7987995172643));
#14445=CARTESIAN_POINT('Ctrl Pts',(-26.0006365353892,21.4569851132792,-57.7982240101578));
#14446=CARTESIAN_POINT('Ctrl Pts',(-25.9969191202143,21.4526413059168,-57.7978718173583));
#14447=CARTESIAN_POINT('Ctrl Pts',(-25.9814923110168,21.434711849466,-57.7964127934644));
#14448=CARTESIAN_POINT('Ctrl Pts',(-25.9696813419681,21.4212143794269,-57.795301748132));
#14449=CARTESIAN_POINT('Ctrl Pts',(-25.8904338557997,21.3321621106129,-57.7878855502183));
#14450=CARTESIAN_POINT('Ctrl Pts',(-25.8195874607473,21.2597309674257,-57.7814359189196));
#14451=CARTESIAN_POINT('Ctrl Pts',(-25.6361430800605,21.0890596460294,-57.7651428214455));
#14452=CARTESIAN_POINT('Ctrl Pts',(-25.5199063930145,20.9950881138442,-57.7551540095863));
#14453=CARTESIAN_POINT('Ctrl Pts',(-25.3100390879029,20.8482746558424,-57.7378481245175));
#14454=CARTESIAN_POINT('Ctrl Pts',(-25.2194989035662,20.7914212427613,-57.7305925085159));
#14455=CARTESIAN_POINT('Ctrl Pts',(-25.0062494922734,20.6718617890272,-57.7141659010924));
#14456=CARTESIAN_POINT('Ctrl Pts',(-24.8819919540363,20.6123041691172,-57.7050601686616));
#14457=CARTESIAN_POINT('Ctrl Pts',(-24.7462495499219,20.5576309623248,-57.6958637039497));
#14458=CARTESIAN_POINT('Ctrl Pts',(-24.7381945573947,20.554424353584,-57.6953207288191));
#14459=CARTESIAN_POINT('Ctrl Pts',(-24.727221300173,20.5501072305708,-57.6945848630776));
#14460=CARTESIAN_POINT('Ctrl Pts',(-24.7243143128069,20.5489684324868,-57.6943902848737));
#14461=CARTESIAN_POINT('Ctrl Pts',(-24.7197192245325,20.5471760269002,-57.6940832944282));
#14462=CARTESIAN_POINT('Ctrl Pts',(-24.7180322295726,20.5465196180406,-57.6939707124067));
#14463=CARTESIAN_POINT('Ctrl Pts',(-24.7146254793751,20.545197357142,-57.6937436124379));
#14464=CARTESIAN_POINT('Ctrl Pts',(-24.7129057176298,20.5445315644982,-57.6936290989763));
#14465=CARTESIAN_POINT('Ctrl Pts',(-24.7089590145325,20.543007522567,-57.6933665947186));
#14466=CARTESIAN_POINT('Ctrl Pts',(-24.7067316931186,20.5421502715355,-57.6932186649969));
#14467=CARTESIAN_POINT('Ctrl Pts',(-24.7020507657025,20.5403546445047,-57.6929082229934));
#14468=CARTESIAN_POINT('Ctrl Pts',(-24.699596958773,20.5394167920313,-57.6927457423099));
#14469=CARTESIAN_POINT('Ctrl Pts',(-24.6931013850175,20.5369432619664,-57.692316306579));
#14470=CARTESIAN_POINT('Ctrl Pts',(-24.6890576526031,20.5354127094695,-57.6920496564556));
#14471=CARTESIAN_POINT('Ctrl Pts',(-24.6768789234974,20.5308310602049,-57.6912486097138));
#14472=CARTESIAN_POINT('Ctrl Pts',(-24.6687345767766,20.5278046879722,-57.6907156537449));
#14473=CARTESIAN_POINT('Ctrl Pts',(-24.5734787401987,20.4928461579931,-57.6845129884456));
#14474=CARTESIAN_POINT('Ctrl Pts',(-24.48503039339,20.4646537972988,-57.6790531313585));
#14475=CARTESIAN_POINT('Ctrl Pts',(-24.012545636256,20.336240566193,-57.6508460337371));
#14476=CARTESIAN_POINT('Ctrl Pts',(-23.6136996045438,20.3037761247706,-57.6298371751098));
#14477=CARTESIAN_POINT('Ctrl Pts',(-23.2005573627612,20.34647794738,-57.6046907376465));
#14478=CARTESIAN_POINT('Ctrl Pts',(-23.1822130988667,20.3485334228294,-57.6035682954636));
#14479=CARTESIAN_POINT('Ctrl Pts',(-23.1579194144522,20.3514670702012,-57.6020736848084));
#14480=CARTESIAN_POINT('Ctrl Pts',(-23.1519530920721,20.3522044927857,-57.6017059696347));
#14481=CARTESIAN_POINT('Ctrl Pts',(-23.1426819877305,20.3533767248028,-57.601133550244));
#14482=CARTESIAN_POINT('Ctrl Pts',(-23.1393757363282,20.3537999773943,-57.6009292119538));
#14483=CARTESIAN_POINT('Ctrl Pts',(-23.1327498146057,20.3546586504959,-57.6005192972483));
#14484=CARTESIAN_POINT('Ctrl Pts',(-23.1294301543508,20.3550941163849,-57.6003137196296));
#14485=CARTESIAN_POINT('Ctrl Pts',(-23.1220088941542,20.3560793875374,-57.5998536780535));
#14486=CARTESIAN_POINT('Ctrl Pts',(-23.1179076679623,20.3566319207738,-57.599599127983));
#14487=CARTESIAN_POINT('Ctrl Pts',(-23.1058806277696,20.3582758426691,-57.5988517133326));
#14488=CARTESIAN_POINT('Ctrl Pts',(-23.0979578431193,20.3593888421716,-57.5983581645011));
#14489=CARTESIAN_POINT('Ctrl Pts',(-23.0387947472441,20.3679248976131,-57.5946635942759));
#14490=CARTESIAN_POINT('Ctrl Pts',(-22.9877383568938,20.376551925934,-57.5914245306387));
#14491=CARTESIAN_POINT('Ctrl Pts',(-22.819517464538,20.4091629497408,-57.5805752693912));
#14492=CARTESIAN_POINT('Ctrl Pts',(-22.7034915364954,20.4384351103793,-57.5728009439833));
#14493=CARTESIAN_POINT('Ctrl Pts',(-22.2941034905325,20.5663127958848,-57.5443653089498));
#14494=CARTESIAN_POINT('Ctrl Pts',(-22.0136788645596,20.7005624071872,-57.5228118047724));
#14495=CARTESIAN_POINT('Ctrl Pts',(-21.728581975593,20.8915350326729,-57.5007993766879));
#14496=CARTESIAN_POINT('Ctrl Pts',(-21.7007679999795,20.9108075999331,-57.4986528704942));
#14497=CARTESIAN_POINT('Ctrl Pts',(-21.6691364050592,20.9334710293991,-57.4962177120585));
#14498=CARTESIAN_POINT('Ctrl Pts',(-21.6650183868341,20.9364362541925,-57.4959008046928));
#14499=CARTESIAN_POINT('Ctrl Pts',(-21.6589606056353,20.940819990431,-57.4954348160416));
#14500=CARTESIAN_POINT('Ctrl Pts',(-21.6570154238762,20.9422309461526,-57.495285214742));
#14501=CARTESIAN_POINT('Ctrl Pts',(-21.6535516593666,20.9447493373241,-57.4950188772084));
#14502=CARTESIAN_POINT('Ctrl Pts',(-21.6520324672996,20.9458559255371,-57.4949020820221));
#14503=CARTESIAN_POINT('Ctrl Pts',(-21.648871758811,20.9481624384528,-57.494659128461));
#14504=CARTESIAN_POINT('Ctrl Pts',(-21.6472304139525,20.9493625847192,-57.4945329863535));
#14505=CARTESIAN_POINT('Ctrl Pts',(-21.6429316638636,20.9525120651939,-57.4942026716492));
#14506=CARTESIAN_POINT('Ctrl Pts',(-21.6402761024094,20.9544639301392,-57.4939986759504));
#14507=CARTESIAN_POINT('Ctrl Pts',(-21.6344702724293,20.9587450077169,-57.4935527953278));
#14508=CARTESIAN_POINT('Ctrl Pts',(-21.6313212421829,20.9610759022885,-57.4933110269172));
#14509=CARTESIAN_POINT('Ctrl Pts',(-21.6220833895435,20.9679398195423,-57.4926019760612));
#14510=CARTESIAN_POINT('Ctrl Pts',(-21.6160062717144,20.9724886572243,-57.4921357703781));
#14511=CARTESIAN_POINT('Ctrl Pts',(-21.3886087076729,21.1439569702839,-57.4746977634172));
#14512=CARTESIAN_POINT('Ctrl Pts',(-21.1896874341797,21.3387476870802,-57.4596194661077));
#14513=CARTESIAN_POINT('Ctrl Pts',(-20.9403891245932,21.6553839403455,-57.4370157889658));
#14514=CARTESIAN_POINT('Ctrl Pts',(-20.8684880099266,21.7585914140504,-57.4299007935136));
#14515=CARTESIAN_POINT('Ctrl Pts',(-20.7509398647797,21.9503118378088,-57.4168125305644));
#14516=CARTESIAN_POINT('Ctrl Pts',(-20.7030175716611,22.0372384363882,-57.4109226251206));
#14517=CARTESIAN_POINT('Ctrl Pts',(-20.6550482255922,22.1346264576388,-57.4043148359424));
#14518=CARTESIAN_POINT('Ctrl Pts',(-20.6509493816541,22.1430402531512,-57.4037439089759));
#14519=CARTESIAN_POINT('Ctrl Pts',(-20.6449219586856,22.1555510126584,-57.4028948606907));
#14520=CARTESIAN_POINT('Ctrl Pts',(-20.6429652453561,22.1596344317056,-57.4026177191693));
#14521=CARTESIAN_POINT('Ctrl Pts',(-20.6396321081082,22.1666280609066,-57.4021430248748));
#14522=CARTESIAN_POINT('Ctrl Pts',(-20.6382514230955,22.1695362430362,-57.4019456204121));
#14523=CARTESIAN_POINT('Ctrl Pts',(-20.635575278848,22.1751949627429,-57.4015614889778));
#14524=CARTESIAN_POINT('Ctrl Pts',(-20.6342793496017,22.1779452747689,-57.40137477861));
#14525=CARTESIAN_POINT('Ctrl Pts',(-20.6311913432075,22.1845229827326,-57.4009282103254));
#14526=CARTESIAN_POINT('Ctrl Pts',(-20.6294029024605,22.1883520705118,-57.4006682267941));
#14527=CARTESIAN_POINT('Ctrl Pts',(-20.6240713338633,22.1998258748409,-57.3998891165285));
#14528=CARTESIAN_POINT('Ctrl Pts',(-20.6205506702282,22.207480935763,-57.3993692143038));
#14529=CARTESIAN_POINT('Ctrl Pts',(-20.5903277807706,22.2738799770066,-57.3948586574146));
#14530=CARTESIAN_POINT('Ctrl Pts',(-20.5653670992528,22.3333961675514,-57.3908085111017));
#14531=CARTESIAN_POINT('Ctrl Pts',(-20.506155759911,22.4873862029339,-57.3802998529767));
#14532=CARTESIAN_POINT('Ctrl Pts',(-20.4745080522996,22.5827802721712,-57.3737607350352));
#14533=CARTESIAN_POINT('Ctrl Pts',(-20.3567110821023,23.0025386569778,-57.3449054566561));
#14534=CARTESIAN_POINT('Ctrl Pts',(-20.3170631103982,23.3377308047378,-57.3214055662827));
#14535=CARTESIAN_POINT('Ctrl Pts',(-20.3301496682481,23.6810996932893,-57.2996748490436));
#14536=CARTESIAN_POINT('Ctrl Pts',(-20.3304893985411,23.6892086416565,-57.2991631426277));
#14537=CARTESIAN_POINT('Ctrl Pts',(-20.3312587739982,23.7060511412434,-57.2981035163414));
#14538=CARTESIAN_POINT('Ctrl Pts',(-20.3316933386075,23.7147844241825,-57.2975558610218));
#14539=CARTESIAN_POINT('Ctrl Pts',(-20.3323318924463,23.7266445338131,-57.2968146552923));
#14540=CARTESIAN_POINT('Ctrl Pts',(-20.3325048999708,23.7297728861042,-57.2966193859177));
#14541=CARTESIAN_POINT('Ctrl Pts',(-20.3327851870622,23.7347104767502,-57.2963115681221));
#14542=CARTESIAN_POINT('Ctrl Pts',(-20.3328894306236,23.7365198749853,-57.2961988483285));
#14543=CARTESIAN_POINT('Ctrl Pts',(-20.3331027740619,23.7401693482807,-57.2959716627221));
#14544=CARTESIAN_POINT('Ctrl Pts',(-20.3332119255056,23.7420094048535,-57.2958572011021));
#14545=CARTESIAN_POINT('Ctrl Pts',(-20.3334658423222,23.7462286501566,-57.2955949340977));
#14546=CARTESIAN_POINT('Ctrl Pts',(-20.3336116683866,23.7486077698811,-57.2954471894972));
#14547=CARTESIAN_POINT('Ctrl Pts',(-20.3339233397548,23.753601879357,-57.2951373440618));
#14548=CARTESIAN_POINT('Ctrl Pts',(-20.3340897351217,23.7562168348512,-57.2949752742858));
#14549=CARTESIAN_POINT('Ctrl Pts',(-20.3345381102975,23.7631301438645,-57.2945472377938));
#14550=CARTESIAN_POINT('Ctrl Pts',(-20.3348255203135,23.7674281581569,-57.2942815733455));
#14551=CARTESIAN_POINT('Ctrl Pts',(-20.3357155924198,23.7803493601208,-57.2934842092417));
#14552=CARTESIAN_POINT('Ctrl Pts',(-20.3363443378491,23.7889707963507,-57.2929539345866));
#14553=CARTESIAN_POINT('Ctrl Pts',(-20.3387148749443,23.8197672819457,-57.291065679137));
#14554=CARTESIAN_POINT('Ctrl Pts',(-20.3406515865325,23.8419272744109,-57.2897179519423));
#14555=CARTESIAN_POINT('Ctrl Pts',(-20.3512547635775,23.9503005297699,-57.2831730026734));
#14556=CARTESIAN_POINT('Ctrl Pts',(-20.3631669343424,24.0361672154874,-57.2781299364639));
#14557=CARTESIAN_POINT('Ctrl Pts',(-20.4293570210763,24.4037013250535,-57.2567680036013));
#14558=CARTESIAN_POINT('Ctrl Pts',(-20.5176305714375,24.6778965084725,-57.2412827874244));
#14559=CARTESIAN_POINT('Ctrl Pts',(-20.6510900054019,24.9579177254986,-57.2232681434173));
#14560=CARTESIAN_POINT('Ctrl Pts',(-20.6613826500207,24.9789216404946,-57.2219034821732));
#14561=CARTESIAN_POINT('Ctrl Pts',(-20.6797923269155,25.0154772380762,-57.2195033325018));
#14562=CARTESIAN_POINT('Ctrl Pts',(-20.6878094617993,25.0310782752427,-57.218470908338));
#14563=CARTESIAN_POINT('Ctrl Pts',(-20.7030611302348,25.0601707482639,-57.2165298340016));
#14564=CARTESIAN_POINT('Ctrl Pts',(-20.7102652325311,25.0736776288064,-57.2156221770147));
#14565=CARTESIAN_POINT('Ctrl Pts',(-20.7208535227341,25.0931933462975,-57.2143010298495));
#14566=CARTESIAN_POINT('Ctrl Pts',(-20.7241612657107,25.0992435789692,-57.213890088024));
#14567=CARTESIAN_POINT('Ctrl Pts',(-20.7336164126128,25.1164070032649,-57.2127203952999));
#14568=CARTESIAN_POINT('Ctrl Pts',(-20.7398100789989,25.1274944501749,-57.211960088756));
#14569=CARTESIAN_POINT('Ctrl Pts',(-20.7522366136755,25.1494339144085,-57.2104460750095));
#14570=CARTESIAN_POINT('Ctrl Pts',(-20.7584674786793,25.1602868118865,-57.2096924469618));
#14571=CARTESIAN_POINT('Ctrl Pts',(-20.7760776391612,25.1905505204419,-57.2075775359374));
#14572=CARTESIAN_POINT('Ctrl Pts',(-20.7875970715632,25.2098785724109,-57.2062113094488));
#14573=CARTESIAN_POINT('Ctrl Pts',(-20.8027026205229,25.2346305383252,-57.2044409813238));
#14574=CARTESIAN_POINT('Ctrl Pts',(-20.8061042629456,25.2401667489687,-57.2040436684296));
#14575=CARTESIAN_POINT('Ctrl Pts',(-20.8115282184863,25.2489347364223,-57.2034122653995));
#14576=CARTESIAN_POINT('Ctrl Pts',(-20.8135395759915,25.25217329786,-57.2031785801177));
#14577=CARTESIAN_POINT('Ctrl Pts',(-20.8173119525095,25.258223362506,-57.2027411434019));
#14578=CARTESIAN_POINT('Ctrl Pts',(-20.8190715770952,25.2610357328517,-57.2025374438066));
#14579=CARTESIAN_POINT('Ctrl Pts',(-20.8230367193929,25.2673514261242,-57.2020791925076));
#14580=CARTESIAN_POINT('Ctrl Pts',(-20.8252446481651,25.2708532217346,-57.2018245515197));
#14581=CARTESIAN_POINT('Ctrl Pts',(-20.8317432178825,25.2811161298966,-57.2010766116614));
#14582=CARTESIAN_POINT('Ctrl Pts',(-20.8360522949027,25.2878654798529,-57.2005826270738));
#14583=CARTESIAN_POINT('Ctrl Pts',(-20.8685091142102,25.3382876023529,-57.1968763195368));
#14584=CARTESIAN_POINT('Ctrl Pts',(-20.8976827744067,25.381287852067,-57.1936256809604));
#14585=CARTESIAN_POINT('Ctrl Pts',(-20.9977911958089,25.521425600096,-57.1827204494532));
#14586=CARTESIAN_POINT('Ctrl Pts',(-21.0731160482794,25.6152879391684,-57.1748996790681));
#14587=CARTESIAN_POINT('Ctrl Pts',(-21.1776884934823,25.7316205482661,-57.1645260543051));
#14588=CARTESIAN_POINT('Ctrl Pts',(-21.2023261213394,25.7581175638018,-57.1621140032997));
#14589=CARTESIAN_POINT('Ctrl Pts',(-21.4160230430489,25.9803192866191,-57.1414740851199));
#14590=CARTESIAN_POINT('Ctrl Pts',(-21.6287181049323,26.1517656440395,-57.1226483325613));
#14591=CARTESIAN_POINT('Ctrl Pts',(-21.8892242215592,26.312180520093,-57.1030232876302));
#14592=CARTESIAN_POINT('Ctrl Pts',(-21.9182997922899,26.3294595665319,-57.1008778232789));
#14593=CARTESIAN_POINT('Ctrl Pts',(-21.9520452983774,26.3488016101807,-57.0984437246965));
#14594=CARTESIAN_POINT('Ctrl Pts',(-21.9564532118967,26.3513143008052,-57.0981268625543));
#14595=CARTESIAN_POINT('Ctrl Pts',(-21.9629574077639,26.3550016338165,-57.0976609276824));
#14596=CARTESIAN_POINT('Ctrl Pts',(-21.9650490716616,26.3561843424658,-57.09751133511));
#14597=CARTESIAN_POINT('Ctrl Pts',(-21.9687791354011,26.3582879644669,-57.0972450074932));
#14598=CARTESIAN_POINT('Ctrl Pts',(-21.9704170180351,26.3592097839042,-57.0971282135124));
#14599=CARTESIAN_POINT('Ctrl Pts',(-21.9738285945352,26.3611259310968,-57.0968852568727));
#14600=CARTESIAN_POINT('Ctrl Pts',(-21.9756024186937,26.3621200105771,-57.0967591104904));
#14601=CARTESIAN_POINT('Ctrl Pts',(-21.9802511101813,26.3647194334157,-57.09642897707));
#14602=CARTESIAN_POINT('Ctrl Pts',(-21.9831275084096,26.3663220560604,-57.0962251664038));
#14603=CARTESIAN_POINT('Ctrl Pts',(-21.9894300107646,26.3698209303043,-57.0957795917737));
#14604=CARTESIAN_POINT('Ctrl Pts',(-21.9928571309974,26.3717153548678,-57.0955379444333));
#14605=CARTESIAN_POINT('Ctrl Pts',(-22.0029332534682,26.3772612256234,-57.0948293362556));
#14606=CARTESIAN_POINT('Ctrl Pts',(-22.0095917608614,26.3808954791918,-57.0943634505653));
#14607=CARTESIAN_POINT('Ctrl Pts',(-22.032646838274,26.3933736298774,-57.0927583035312));
#14608=CARTESIAN_POINT('Ctrl Pts',(-22.0491075775814,26.4020990358464,-57.0916261722981));
#14609=CARTESIAN_POINT('Ctrl Pts',(-22.0687716968809,26.4123050330163,-57.0902890711953));
#14610=CARTESIAN_POINT('Ctrl Pts',(-22.0719025437825,26.413923479465,-57.0900766428938));
#14611=CARTESIAN_POINT('Ctrl Pts',(-22.0750360153845,26.415536774576,-57.0898644896988));
#14612=CARTESIAN_POINT('Origin',(-23.5502525316942,23.5502525316942,-77.3107734492734));
#14613=CARTESIAN_POINT('',(-22.0750357439087,26.4155366348044,-55.5940940905006));
#14614=CARTESIAN_POINT('',(-22.0750360153461,26.4155367745563,-55.8427674868566));
#14615=CARTESIAN_POINT('',(-22.0750360153461,26.4155367745563,-77.3107734492734));
#14616=CARTESIAN_POINT('',(-26.7730018744143,23.5523108070312,-56.4368032791696));
#14617=CARTESIAN_POINT('Ctrl Pts',(-22.0750357439015,26.4155366348007,-55.5940940905011));
#14618=CARTESIAN_POINT('Ctrl Pts',(-21.9838795594224,26.3686040693672,-55.600025320068));
#14619=CARTESIAN_POINT('Ctrl Pts',(-21.8948657812043,26.3172716490372,-55.6060829891755));
#14620=CARTESIAN_POINT('Ctrl Pts',(-21.7924440880926,26.2514713208581,-55.6134516178906));
#14621=CARTESIAN_POINT('Ctrl Pts',(-21.7766619380222,26.2411352593132,-55.6145986091763));
#14622=CARTESIAN_POINT('Ctrl Pts',(-21.7559279749849,26.2272945042548,-55.6161211799293));
#14623=CARTESIAN_POINT('Ctrl Pts',(-21.7508937870136,26.2239134011405,-55.6164920932773));
#14624=CARTESIAN_POINT('Ctrl Pts',(-21.7430987173382,26.2186460248088,-55.6170683558746));
#14625=CARTESIAN_POINT('Ctrl Pts',(-21.7403311590718,26.2167696172624,-55.6172733309547));
#14626=CARTESIAN_POINT('Ctrl Pts',(-21.7348548922085,26.2130442488274,-55.6176796765315));
#14627=CARTESIAN_POINT('Ctrl Pts',(-21.7321460754695,26.2111954532902,-55.6178810405864));
#14628=CARTESIAN_POINT('Ctrl Pts',(-21.7261388697134,26.2070820178816,-55.6183284126075));
#14629=CARTESIAN_POINT('Ctrl Pts',(-21.7228418704403,26.2048153667773,-55.6185744970169));
#14630=CARTESIAN_POINT('Ctrl Pts',(-21.7160026982318,26.2000947307717,-55.619086109891));
#14631=CARTESIAN_POINT('Ctrl Pts',(-21.7124612110051,26.1976397706299,-55.6193516753463));
#14632=CARTESIAN_POINT('Ctrl Pts',(-21.7033622813481,26.1913053333773,-55.620035631653));
#14633=CARTESIAN_POINT('Ctrl Pts',(-21.6978121547805,26.1874154290053,-55.6204544219746));
#14634=CARTESIAN_POINT('Ctrl Pts',(-21.6817334517017,26.1760705827888,-55.6216723180834));
#14635=CARTESIAN_POINT('Ctrl Pts',(-21.6712374087872,26.1685699589431,-55.6224731810303));
#14636=CARTESIAN_POINT('Ctrl Pts',(-21.5668551882934,26.0930260269633,-55.6304966927973));
#14637=CARTESIAN_POINT('Ctrl Pts',(-21.4766717069034,26.0200337264738,-55.6379128419842));
#14638=CARTESIAN_POINT('Ctrl Pts',(-21.1504964090363,25.7255567690064,-55.6666665889065));
#14639=CARTESIAN_POINT('Ctrl Pts',(-20.944420698649,25.4738878582367,-55.6892117691785));
#14640=CARTESIAN_POINT('Ctrl Pts',(-20.7751131358962,25.1887839529248,-55.7108085320634));
#14641=CARTESIAN_POINT('Ctrl Pts',(-20.7709814193324,25.1817659306554,-55.7113377934035));
#14642=CARTESIAN_POINT('Ctrl Pts',(-20.7414883524118,25.1312326430257,-55.7151314461384));
#14643=CARTESIAN_POINT('Ctrl Pts',(-20.7171218053369,25.0871407266879,-55.7183497322672));
#14644=CARTESIAN_POINT('Ctrl Pts',(-20.6914311426112,25.0379635051749,-55.7218244622239));
#14645=CARTESIAN_POINT('Ctrl Pts',(-20.6890757680994,25.0334285844984,-55.7221438281986));
#14646=CARTESIAN_POINT('Ctrl Pts',(-20.6855864519968,25.0266711847788,-55.7226181131022));
#14647=CARTESIAN_POINT('Ctrl Pts',(-20.684444303259,25.0244529879692,-55.7227735473916));
#14648=CARTESIAN_POINT('Ctrl Pts',(-20.6824896390722,25.0206459276338,-55.7230398764086));
#14649=CARTESIAN_POINT('Ctrl Pts',(-20.6816758676216,25.0190577160178,-55.7231508509402));
#14650=CARTESIAN_POINT('Ctrl Pts',(-20.680087794635,25.0159519712353,-55.723367603543));
#14651=CARTESIAN_POINT('Ctrl Pts',(-20.6793133791906,25.0144345038414,-55.7234733885449));
#14652=CARTESIAN_POINT('Ctrl Pts',(-20.6774386704505,25.0107538056879,-55.7237296853884));
#14653=CARTESIAN_POINT('Ctrl Pts',(-20.6763396141801,25.008589939611,-55.7238801183483));
#14654=CARTESIAN_POINT('Ctrl Pts',(-20.6729546872348,25.0019068724516,-55.7243439855108));
#14655=CARTESIAN_POINT('Ctrl Pts',(-20.6706770098204,24.9973834951613,-55.7246569029238));
#14656=CARTESIAN_POINT('Ctrl Pts',(-20.6450974636079,24.9462840135437,-55.7281802636299));
#14657=CARTESIAN_POINT('Ctrl Pts',(-20.6229155803774,24.8991517159277,-55.7313216004657));
#14658=CARTESIAN_POINT('Ctrl Pts',(-20.5785195256159,24.7985590176384,-55.7378425248174));
#14659=CARTESIAN_POINT('Ctrl Pts',(-20.5565834619849,24.7449961756656,-55.7412086701161));
#14660=CARTESIAN_POINT('Ctrl Pts',(-20.3990756803858,24.3287717520528,-55.7667686977408));
#14661=CARTESIAN_POINT('Ctrl Pts',(-20.3284139178172,23.9449678815775,-55.787339419887));
#14662=CARTESIAN_POINT('Ctrl Pts',(-20.3274626654681,23.5369074032937,-55.8120101374411));
#14663=CARTESIAN_POINT('Ctrl Pts',(-20.3276165349103,23.5160499769984,-55.8132773581588));
#14664=CARTESIAN_POINT('Ctrl Pts',(-20.3280806442961,23.4888872201346,-55.8149362135786));
#14665=CARTESIAN_POINT('Ctrl Pts',(-20.3282069617768,23.4825789187939,-55.8153220676715));
#14666=CARTESIAN_POINT('Ctrl Pts',(-20.3284296962321,23.4728788097124,-55.8159163214658));
#14667=CARTESIAN_POINT('Ctrl Pts',(-20.3285129465119,23.469486690595,-55.8161243075208));
#14668=CARTESIAN_POINT('Ctrl Pts',(-20.3286806367598,23.4630673287175,-55.8165182430365));
#14669=CARTESIAN_POINT('Ctrl Pts',(-20.3287639870076,23.4600400591522,-55.8167041580671));
#14670=CARTESIAN_POINT('Ctrl Pts',(-20.3289623512292,23.4531866341488,-55.8171253722893));
#14671=CARTESIAN_POINT('Ctrl Pts',(-20.3290799151622,23.4493605620969,-55.8173607513237));
#14672=CARTESIAN_POINT('Ctrl Pts',(-20.3294212755269,23.4388605506749,-55.8180073375857));
#14673=CARTESIAN_POINT('Ctrl Pts',(-20.3296589979729,23.4321871107737,-55.8184189817236));
#14674=CARTESIAN_POINT('Ctrl Pts',(-20.3302319373418,23.417395657934,-55.8193329402021));
#14675=CARTESIAN_POINT('Ctrl Pts',(-20.3305771158,23.4092780967719,-55.8198355655231));
#14676=CARTESIAN_POINT('Ctrl Pts',(-20.3317171308859,23.3846618472474,-55.8213629716101));
#14677=CARTESIAN_POINT('Ctrl Pts',(-20.3326081080357,23.3681680800315,-55.822390765675));
#14678=CARTESIAN_POINT('Ctrl Pts',(-20.3362702147324,23.3088458930996,-55.82610349676));
#14679=CARTESIAN_POINT('Ctrl Pts',(-20.3397699111697,23.2660685131726,-55.8288110991634));
#14680=CARTESIAN_POINT('Ctrl Pts',(-20.3543571818757,23.1229912646559,-55.8379724806893));
#14681=CARTESIAN_POINT('Ctrl Pts',(-20.3692996213143,23.0231524416621,-55.8445415419931));
#14682=CARTESIAN_POINT('Ctrl Pts',(-20.449093655949,22.6202281378749,-55.8717324764799));
#14683=CARTESIAN_POINT('Ctrl Pts',(-20.5528010600627,22.3265702393382,-55.8933218829525));
#14684=CARTESIAN_POINT('Ctrl Pts',(-20.714522577222,22.0185202148446,-55.9157053549482));
#14685=CARTESIAN_POINT('Ctrl Pts',(-20.7328242457011,21.9851115038259,-55.9181262676892));
#14686=CARTESIAN_POINT('Ctrl Pts',(-20.7543199458152,21.9474717819182,-55.9208394323022));
#14687=CARTESIAN_POINT('Ctrl Pts',(-20.7569361789822,21.9429165645628,-55.9211675412091));
#14688=CARTESIAN_POINT('Ctrl Pts',(-20.7607825226993,21.9362573113983,-55.9216468235589));
#14689=CARTESIAN_POINT('Ctrl Pts',(-20.7620038836986,21.934148271671,-55.9217985604257));
#14690=CARTESIAN_POINT('Ctrl Pts',(-20.7641737719267,21.9304111020053,-55.9220673328983));
#14691=CARTESIAN_POINT('Ctrl Pts',(-20.7651213350593,21.9287824177024,-55.9221844313966));
#14692=CARTESIAN_POINT('Ctrl Pts',(-20.76710660648,21.9253769810468,-55.9224292011152));
#14693=CARTESIAN_POINT('Ctrl Pts',(-20.768144585776,21.923600395113,-55.9225568539366));
#14694=CARTESIAN_POINT('Ctrl Pts',(-20.7708676266075,21.9189499201307,-55.9228908988748));
#14695=CARTESIAN_POINT('Ctrl Pts',(-20.7725554497548,21.9160776382567,-55.9230971104453));
#14696=CARTESIAN_POINT('Ctrl Pts',(-20.7799799241102,21.9034876472217,-55.9240005529012));
#14697=CARTESIAN_POINT('Ctrl Pts',(-20.7857632305311,21.8937973352767,-55.9246947692464));
#14698=CARTESIAN_POINT('Ctrl Pts',(-20.8285059523694,21.8230264574653,-55.9297578875546));
#14699=CARTESIAN_POINT('Ctrl Pts',(-20.8674382103166,21.7631533612404,-55.9340034961394));
#14700=CARTESIAN_POINT('Ctrl Pts',(-20.9357895673577,21.665312236726,-55.9409637089057));
#14701=CARTESIAN_POINT('Ctrl Pts',(-20.9641232964571,21.626622517405,-55.9437221583312));
#14702=CARTESIAN_POINT('Ctrl Pts',(-21.0149621293702,21.5603567145551,-55.9484840212353));
#14703=CARTESIAN_POINT('Ctrl Pts',(-21.0370795819349,21.5324952114008,-55.9504981341233));
#14704=CARTESIAN_POINT('Ctrl Pts',(-21.2452199372087,21.2790324626451,-55.9689876976082));
#14705=CARTESIAN_POINT('Ctrl Pts',(-21.4606560863423,21.0793829418304,-55.9849398400474));
#14706=CARTESIAN_POINT('Ctrl Pts',(-21.7054336156591,20.9077529964041,-56.002673309641));
#14707=CARTESIAN_POINT('Ctrl Pts',(-21.7108182228074,20.9040019673382,-56.0030631544036));
#14708=CARTESIAN_POINT('Ctrl Pts',(-21.7218658596289,20.8963559661733,-56.00386251072));
#14709=CARTESIAN_POINT('Ctrl Pts',(-21.7275299647967,20.8924626140867,-56.0042720768863));
#14710=CARTESIAN_POINT('Ctrl Pts',(-21.7702842403175,20.8632754376662,-56.007361751677));
#14711=CARTESIAN_POINT('Ctrl Pts',(-21.8078853683745,20.8387419966433,-56.0100686931956));
#14712=CARTESIAN_POINT('Ctrl Pts',(-21.8523192132048,20.8110563536344,-56.0132602154625));
#14713=CARTESIAN_POINT('Ctrl Pts',(-21.8586667766723,20.8071318839892,-56.0137159640924));
#14714=CARTESIAN_POINT('Ctrl Pts',(-21.8688138900393,20.800906903123,-56.0144442630828));
#14715=CARTESIAN_POINT('Ctrl Pts',(-21.8726046902539,20.7985921219068,-56.0147162878173));
#14716=CARTESIAN_POINT('Ctrl Pts',(-21.8793014143235,20.7945218750601,-56.0151967454117));
#14717=CARTESIAN_POINT('Ctrl Pts',(-21.8822053555841,20.7927631470027,-56.015405058119));
#14718=CARTESIAN_POINT('Ctrl Pts',(-21.8881504567554,20.7891754141683,-56.0158314659655));
#14719=CARTESIAN_POINT('Ctrl Pts',(-21.8911918686809,20.7873468379141,-56.0160495764252));
#14720=CARTESIAN_POINT('Ctrl Pts',(-21.8989165664418,20.7827199020024,-56.0166034631081));
#14721=CARTESIAN_POINT('Ctrl Pts',(-21.903603935679,20.7799284121731,-56.016939489811));
#14722=CARTESIAN_POINT('Ctrl Pts',(-21.9137592969406,20.7739154246187,-56.0176673561702));
#14723=CARTESIAN_POINT('Ctrl Pts',(-21.9192297538918,20.7706981543014,-56.0180593483607));
#14724=CARTESIAN_POINT('Ctrl Pts',(-21.9348854697905,20.7615528887393,-56.019180933954));
#14725=CARTESIAN_POINT('Ctrl Pts',(-21.9450937097022,20.7556646204742,-56.019911965692));
#14726=CARTESIAN_POINT('Ctrl Pts',(-21.9790265452408,20.7363389080943,-56.0223411272367));
#14727=CARTESIAN_POINT('Ctrl Pts',(-22.0028888593446,20.7231468433,-56.0240480354534));
#14728=CARTESIAN_POINT('Ctrl Pts',(-22.0990714558389,20.6715556792098,-56.0309243336377));
#14729=CARTESIAN_POINT('Ctrl Pts',(-22.1726709117516,20.6356189265752,-56.036178699719));
#14730=CARTESIAN_POINT('Ctrl Pts',(-22.513364249961,20.4850551859137,-56.0604706658564));
#14731=CARTESIAN_POINT('Ctrl Pts',(-22.7938364264267,20.4040856826114,-56.0805441675637));
#14732=CARTESIAN_POINT('Ctrl Pts',(-23.1171472288634,20.3565319184216,-56.1022340171842));
#14733=CARTESIAN_POINT('Ctrl Pts',(-23.1530981791113,20.3518622865729,-56.1046237584023));
#14734=CARTESIAN_POINT('Ctrl Pts',(-23.1954859148836,20.3470823470667,-56.1074099896367));
#14735=CARTESIAN_POINT('Ctrl Pts',(-23.2018525573201,20.3463836137882,-56.1078276503416));
#14736=CARTESIAN_POINT('Ctrl Pts',(-23.2124239645604,20.3452552952761,-56.1085197256729));
#14737=CARTESIAN_POINT('Ctrl Pts',(-23.2166275423312,20.3448149963424,-56.1087945466895));
#14738=CARTESIAN_POINT('Ctrl Pts',(-23.2737291353791,20.3389474970378,-56.1125225529528));
#14739=CARTESIAN_POINT('Ctrl Pts',(-23.3267566801838,20.3348216669469,-56.1159243645876));
#14740=CARTESIAN_POINT('Ctrl Pts',(-23.3856153410031,20.3317054513409,-56.1196160004429));
#14741=CARTESIAN_POINT('Ctrl Pts',(-23.3913657948243,20.33141645027,-56.1199757803214));
#14742=CARTESIAN_POINT('Ctrl Pts',(-23.3994171940089,20.3310334391093,-56.1204782440544));
#14743=CARTESIAN_POINT('Ctrl Pts',(-23.4017174684382,20.330926484177,-56.1206216515405));
#14744=CARTESIAN_POINT('Ctrl Pts',(-23.4059245561861,20.330735387624,-56.1208836677018));
#14745=CARTESIAN_POINT('Ctrl Pts',(-23.4078313321111,20.3306504743829,-56.1210023200823));
#14746=CARTESIAN_POINT('Ctrl Pts',(-23.41170234964,20.3304815344301,-56.1212429940806));
#14747=CARTESIAN_POINT('Ctrl Pts',(-23.4136665933762,20.3303976111623,-56.1213650097029));
#14748=CARTESIAN_POINT('Ctrl Pts',(-23.4185439561983,20.3301936946138,-56.121667718288));
#14749=CARTESIAN_POINT('Ctrl Pts',(-23.4214571710768,20.3300758566711,-56.1218482890927));
#14750=CARTESIAN_POINT('Ctrl Pts',(-23.432322275103,20.3296511369945,-56.1225208818048));
#14751=CARTESIAN_POINT('Ctrl Pts',(-23.4402752181687,20.3293697516721,-56.1230114769578));
#14752=CARTESIAN_POINT('Ctrl Pts',(-23.5747741654176,20.3251097535378,-56.1312804361758));
#14753=CARTESIAN_POINT('Ctrl Pts',(-23.7014630428073,20.3285617935038,-56.1386528939467));
#14754=CARTESIAN_POINT('Ctrl Pts',(-23.8612734438857,20.3423679452839,-56.1477877469958));
#14755=CARTESIAN_POINT('Ctrl Pts',(-23.8948643509231,20.3458024543773,-56.1496984027349));
#14756=CARTESIAN_POINT('Ctrl Pts',(-23.9558167961334,20.3530040884762,-56.1531574479588));
#14757=CARTESIAN_POINT('Ctrl Pts',(-23.9831954462334,20.3565962509917,-56.1547082548693));
#14758=CARTESIAN_POINT('Ctrl Pts',(-24.0338067452319,20.3638994090814,-56.1575745184197));
#14759=CARTESIAN_POINT('Ctrl Pts',(-24.0570513309089,20.3675137919785,-56.1588907251335));
#14760=CARTESIAN_POINT('Ctrl Pts',(-24.1004759911404,20.3747538324374,-56.161352190805));
#14761=CARTESIAN_POINT('Ctrl Pts',(-24.1206650262533,20.3783181956577,-56.1624976250833));
#14762=CARTESIAN_POINT('Ctrl Pts',(-24.1586403638953,20.3853970127006,-56.164656043476));
#14763=CARTESIAN_POINT('Ctrl Pts',(-24.1764336700842,20.3888693864078,-56.1656689766118));
#14764=CARTESIAN_POINT('Ctrl Pts',(-24.3635298895736,20.4270228528824,-56.1763439593797));
#14765=CARTESIAN_POINT('Ctrl Pts',(-24.529795748061,20.475114931625,-56.186057826214));
#14766=CARTESIAN_POINT('Ctrl Pts',(-24.7104125811944,20.5435001885044,-56.1973725537662));
#14767=CARTESIAN_POINT('Ctrl Pts',(-24.7293593767706,20.5508795945102,-56.1985689103523));
#14768=CARTESIAN_POINT('Ctrl Pts',(-24.752475383421,20.5601357040109,-56.2000407371455));
#14769=CARTESIAN_POINT('Ctrl Pts',(-24.756712347831,20.5618427304522,-56.2003110153679));
#14770=CARTESIAN_POINT('Ctrl Pts',(-24.7646792606191,20.5650722167106,-56.200820190399));
#14771=CARTESIAN_POINT('Ctrl Pts',(-24.7684100143864,20.5665926750673,-56.2010590250964));
#14772=CARTESIAN_POINT('Ctrl Pts',(-24.775983250039,20.5696956981808,-56.2015446629261));
#14773=CARTESIAN_POINT('Ctrl Pts',(-24.7798255406509,20.5712787071846,-56.2017914795223));
#14774=CARTESIAN_POINT('Ctrl Pts',(-24.7872193095958,20.5743416533091,-56.2022672634635));
#14775=CARTESIAN_POINT('Ctrl Pts',(-24.7907712222886,20.5758205281303,-56.2024961970525));
#14776=CARTESIAN_POINT('Ctrl Pts',(-24.800485075476,20.5798854153247,-56.203123312724));
#14777=CARTESIAN_POINT('Ctrl Pts',(-24.8066416112257,20.5824842288445,-56.203521900151));
#14778=CARTESIAN_POINT('Ctrl Pts',(-24.8141718909226,20.585690562069,-56.2040108288818));
#14779=CARTESIAN_POINT('Ctrl Pts',(-24.8155533826047,20.5862799314405,-56.2041005847826));
#14780=CARTESIAN_POINT('Ctrl Pts',(-24.8232473027992,20.5895686565504,-56.2046007845587));
#14781=CARTESIAN_POINT('Ctrl Pts',(-24.8295514705077,20.5922871972335,-56.2050118474501));
#14782=CARTESIAN_POINT('Ctrl Pts',(-24.8413831799372,20.597434274004,-56.2057856477019));
#14783=CARTESIAN_POINT('Ctrl Pts',(-24.8469126849512,20.5998582427907,-56.2061482340082));
#14784=CARTESIAN_POINT('Ctrl Pts',(-24.8755169572995,20.6124934402352,-56.208028900367));
#14785=CARTESIAN_POINT('Ctrl Pts',(-24.8984775337773,20.6229596585026,-56.2095553934008));
#14786=CARTESIAN_POINT('Ctrl Pts',(-24.9298089692704,20.6376884132013,-56.2116626079141));
#14787=CARTESIAN_POINT('Ctrl Pts',(-24.9382880204995,20.6417197077988,-56.2122353256777));
#14788=CARTESIAN_POINT('Ctrl Pts',(-24.9508365127292,20.6477531532043,-56.2130866048625));
#14789=CARTESIAN_POINT('Ctrl Pts',(-24.9549195906399,20.6497269615196,-56.2133641793519));
#14790=CARTESIAN_POINT('Ctrl Pts',(-24.9618955348806,20.653117400299,-56.2138394173272));
#14791=CARTESIAN_POINT('Ctrl Pts',(-24.9647904770672,20.6545297654411,-56.214036931732));
#14792=CARTESIAN_POINT('Ctrl Pts',(-24.9705918922675,20.6573708970113,-56.2144333429391));
#14793=CARTESIAN_POINT('Ctrl Pts',(-24.9734983380794,20.6587997089826,-56.2146322411362));
#14794=CARTESIAN_POINT('Ctrl Pts',(-24.980202942142,20.6621082580098,-56.2150917571967));
#14795=CARTESIAN_POINT('Ctrl Pts',(-24.983999549966,20.6639911074156,-56.2153524839062));
#14796=CARTESIAN_POINT('Ctrl Pts',(-24.9954560256224,20.6697008930686,-56.2161408117007));
#14797=CARTESIAN_POINT('Ctrl Pts',(-25.0031043201174,20.6735508509047,-56.2166692207665));
#14798=CARTESIAN_POINT('Ctrl Pts',(-25.0205615029873,20.6824257316408,-56.2178802206822));
#14799=CARTESIAN_POINT('Ctrl Pts',(-25.0303600993239,20.6874705613804,-56.2185635102775));
#14800=CARTESIAN_POINT('Ctrl Pts',(-25.062228180893,20.7040852629906,-56.2207975411282));
#14801=CARTESIAN_POINT('Ctrl Pts',(-25.0841889643059,20.715860630489,-56.2223555405025));
#14802=CARTESIAN_POINT('Ctrl Pts',(-25.171033682565,20.763731633463,-56.2285919426978));
#14803=CARTESIAN_POINT('Ctrl Pts',(-25.2347941438381,20.801807812917,-56.233340290231));
#14804=CARTESIAN_POINT('Ctrl Pts',(-25.3499260299225,20.876073636675,-56.2422361196812));
#14805=CARTESIAN_POINT('Ctrl Pts',(-25.4016650259413,20.9116300693082,-56.2463610268011));
#14806=CARTESIAN_POINT('Ctrl Pts',(-25.6682400166094,21.1065295093652,-56.2682720182018));
#14807=CARTESIAN_POINT('Ctrl Pts',(-25.863640934846,21.2906342932802,-56.2867639652581));
#14808=CARTESIAN_POINT('Ctrl Pts',(-26.0492881014276,21.5151823277497,-56.3058709451657));
#14809=CARTESIAN_POINT('Ctrl Pts',(-26.0643215804226,21.5337837385994,-56.3074302805929));
#14810=CARTESIAN_POINT('Ctrl Pts',(-26.0800290861947,21.5536679049431,-56.3090710349475));
#14811=CARTESIAN_POINT('Ctrl Pts',(-26.0809104407822,21.5547851341495,-56.3091631373156));
#14812=CARTESIAN_POINT('Ctrl Pts',(-26.0864923579264,21.561870571133,-56.3097466981448));
#14813=CARTESIAN_POINT('Ctrl Pts',(-26.0911725884148,21.5678548559452,-56.3102370963472));
#14814=CARTESIAN_POINT('Ctrl Pts',(-26.1200968594941,21.6051090243471,-56.3132744071318));
#14815=CARTESIAN_POINT('Ctrl Pts',(-26.1437858388642,21.6368083925734,-56.3157909711665));
#14816=CARTESIAN_POINT('Ctrl Pts',(-26.1699860921746,21.6732491136832,-56.3186005135982));
#14817=CARTESIAN_POINT('Ctrl Pts',(-26.1730752568516,21.6775681716135,-56.3189322013199));
#14818=CARTESIAN_POINT('Ctrl Pts',(-26.1775729317662,21.6838894720756,-56.3194157233918));
#14819=CARTESIAN_POINT('Ctrl Pts',(-26.1789898374854,21.6858856868429,-56.3195681353772));
#14820=CARTESIAN_POINT('Ctrl Pts',(-26.1814942972349,21.6894226387778,-56.3198376846851));
#14821=CARTESIAN_POINT('Ctrl Pts',(-26.1825827739808,21.6909627170837,-56.3199548861439));
#14822=CARTESIAN_POINT('Ctrl Pts',(-26.1848530176393,21.6941808589483,-56.3201994400194));
#14823=CARTESIAN_POINT('Ctrl Pts',(-26.1860345310423,21.6958590926201,-56.3203267747702));
#14824=CARTESIAN_POINT('Ctrl Pts',(-26.1891163975487,21.7002455031944,-56.3206590768362));
#14825=CARTESIAN_POINT('Ctrl Pts',(-26.1910141912397,21.7029554885201,-56.3208638670555));
#14826=CARTESIAN_POINT('Ctrl Pts',(-26.1992455709247,21.7147482274573,-56.3217528351257));
#14827=CARTESIAN_POINT('Ctrl Pts',(-26.2055365945244,21.7238608084104,-56.3224341166714));
#14828=CARTESIAN_POINT('Ctrl Pts',(-26.250803818078,21.7901588981375,-56.3273513514363));
#14829=CARTESIAN_POINT('Ctrl Pts',(-26.2879793122929,21.8485590945873,-56.331471410409));
#14830=CARTESIAN_POINT('Ctrl Pts',(-26.487626650329,22.1856937876466,-56.354352350173));
#14831=CARTESIAN_POINT('Ctrl Pts',(-26.6094079433382,22.4863923652025,-56.3715432198012));
#14832=CARTESIAN_POINT('Ctrl Pts',(-26.6888556032308,22.818379680284,-56.3913169957944));
#14833=CARTESIAN_POINT('Ctrl Pts',(-26.6930485549052,22.8365997800023,-56.3924039265359));
#14834=CARTESIAN_POINT('Ctrl Pts',(-26.7170541354781,22.9452304444625,-56.3988971574075));
#14835=CARTESIAN_POINT('Ctrl Pts',(-26.7331213899719,23.0364165285247,-56.4044021051064));
#14836=CARTESIAN_POINT('Ctrl Pts',(-26.7465800634763,23.1382910401125,-56.4106575834641));
#14837=CARTESIAN_POINT('Ctrl Pts',(-26.7478700879922,23.1484267972651,-56.4112810829464));
#14838=CARTESIAN_POINT('Ctrl Pts',(-26.7496120859228,23.1626535843466,-56.4121578731054));
#14839=CARTESIAN_POINT('Ctrl Pts',(-26.7501044649097,23.166739681244,-56.4124098858988));
#14840=CARTESIAN_POINT('Ctrl Pts',(-26.7509922159806,23.1742275797011,-56.4128720567723));
#14841=CARTESIAN_POINT('Ctrl Pts',(-26.7513899959649,23.1776290947063,-56.4130821384751));
#14842=CARTESIAN_POINT('Ctrl Pts',(-26.7521429070811,23.1841576112422,-56.4134856035549));
#14843=CARTESIAN_POINT('Ctrl Pts',(-26.7524988813425,23.187284512679,-56.4136789600031));
#14844=CARTESIAN_POINT('Ctrl Pts',(-26.7532330695095,23.1938188206494,-56.4140832556221));
#14845=CARTESIAN_POINT('Ctrl Pts',(-26.7536104274125,23.1972263176715,-56.4142942215946));
#14846=CARTESIAN_POINT('Ctrl Pts',(-26.7544863012855,23.205252398087,-56.4147914548199));
#14847=CARTESIAN_POINT('Ctrl Pts',(-26.754980268767,23.2098714610526,-56.4150778654233));
#14848=CARTESIAN_POINT('Ctrl Pts',(-26.7562537509156,23.2220282636645,-56.4158323268058));
#14849=CARTESIAN_POINT('Ctrl Pts',(-26.7570166658164,23.2295676796906,-56.4163009008134));
#14850=CARTESIAN_POINT('Ctrl Pts',(-26.7679812253469,23.3418768948182,-56.4232910779254));
#14851=CARTESIAN_POINT('Ctrl Pts',(-26.7730690891451,23.4470691876655,-56.429973293957));
#14852=CARTESIAN_POINT('Ctrl Pts',(-26.7730018744143,23.5523108070312,-56.4368032791696));
#14853=CARTESIAN_POINT('Ctrl Pts',(-26.7730018769529,23.5523068283337,-56.4368030209596));
#14854=CARTESIAN_POINT('Ctrl Pts',(-26.772795047506,23.8767777209974,-56.4578605669829));
#14855=CARTESIAN_POINT('Ctrl Pts',(-26.7235944638763,24.1993030980816,-56.4804034481421));
#14856=CARTESIAN_POINT('Ctrl Pts',(-26.6057090741017,24.5776094452741,-56.5064782171832));
#14857=CARTESIAN_POINT('Ctrl Pts',(-26.5820511284921,24.6454584567933,-56.5111274809225));
#14858=CARTESIAN_POINT('Ctrl Pts',(-26.5520584605614,24.7230300120075,-56.5163666614606));
#14859=CARTESIAN_POINT('Ctrl Pts',(-26.5479180592104,24.7335729646986,-56.5170770654102));
#14860=CARTESIAN_POINT('Ctrl Pts',(-26.5424863008555,24.7471926980964,-56.5179924215039));
#14861=CARTESIAN_POINT('Ctrl Pts',(-26.541245697338,24.7502894371971,-56.5182003884329));
#14862=CARTESIAN_POINT('Ctrl Pts',(-26.5392317585472,24.7552940171778,-56.5185362159691));
#14863=CARTESIAN_POINT('Ctrl Pts',(-26.5384614038799,24.7572030429178,-56.518664257155));
#14864=CARTESIAN_POINT('Ctrl Pts',(-26.5369825391173,24.7608577417391,-56.5189092623037));
#14865=CARTESIAN_POINT('Ctrl Pts',(-26.5362743296622,24.7626035262101,-56.5190262437593));
#14866=CARTESIAN_POINT('Ctrl Pts',(-26.5346472300783,24.7666043625157,-56.5192942114077));
#14867=CARTESIAN_POINT('Ctrl Pts',(-26.5337273126147,24.7688589996696,-56.5194451347702));
#14868=CARTESIAN_POINT('Ctrl Pts',(-26.5308190106975,24.7759639601857,-56.5199204648755));
#14869=CARTESIAN_POINT('Ctrl Pts',(-26.5288213340867,24.7808105075839,-56.5202443082064));
#14870=CARTESIAN_POINT('Ctrl Pts',(-26.5123166558212,24.8205767101645,-56.5228983735687));
#14871=CARTESIAN_POINT('Ctrl Pts',(-26.4972071675566,24.8552452802931,-56.5251926344906));
#14872=CARTESIAN_POINT('Ctrl Pts',(-26.4775114027901,24.8983492329477,-56.5280301510296));
#14873=CARTESIAN_POINT('Ctrl Pts',(-26.473493788296,24.9070390935149,-56.5286014292358));
#14874=CARTESIAN_POINT('Ctrl Pts',(-26.4680298672539,24.9187202951576,-56.5293684876796));
#14875=CARTESIAN_POINT('Ctrl Pts',(-26.4666176125471,24.9217274001838,-56.5295658742123));
#14876=CARTESIAN_POINT('Ctrl Pts',(-26.4635963139718,24.9281348634207,-56.5299863047395));
#14877=CARTESIAN_POINT('Ctrl Pts',(-26.4619859597716,24.9315346020478,-56.5302092874632));
#14878=CARTESIAN_POINT('Ctrl Pts',(-26.4591067339186,24.937585740589,-56.5306060172105));
#14879=CARTESIAN_POINT('Ctrl Pts',(-26.4578401834328,24.9402382330135,-56.5307798694545));
#14880=CARTESIAN_POINT('Ctrl Pts',(-26.4000813575423,25.0607761399479,-56.5386780507431));
#14881=CARTESIAN_POINT('Ctrl Pts',(-26.3364669725927,25.1751282683427,-56.5460768510529));
#14882=CARTESIAN_POINT('Ctrl Pts',(-26.1746881567577,25.4283551308489,-56.5629297729614));
#14883=CARTESIAN_POINT('Ctrl Pts',(-26.0721442528753,25.5639536696237,-56.5723214032149));
#14884=CARTESIAN_POINT('Ctrl Pts',(-25.9246523887287,25.7299496403482,-56.5849957302839));
#14885=CARTESIAN_POINT('Ctrl Pts',(-25.8889598993441,25.7682024119219,-56.5880063334643));
#14886=CARTESIAN_POINT('Ctrl Pts',(-25.8040926966018,25.8548301235245,-56.5950622472781));
#14887=CARTESIAN_POINT('Ctrl Pts',(-25.7542661640202,25.9025272343392,-56.5991301921456));
#14888=CARTESIAN_POINT('Ctrl Pts',(-25.6854390088445,25.9643051368157,-56.6046777260879));
#14889=CARTESIAN_POINT('Ctrl Pts',(-25.6677562108489,25.9798305602173,-56.6060968758131));
#14890=CARTESIAN_POINT('Ctrl Pts',(-25.6379599553161,26.0054191665922,-56.6084790618197));
#14891=CARTESIAN_POINT('Ctrl Pts',(-25.625939727593,26.0155898600919,-56.6094376379942));
#14892=CARTESIAN_POINT('Ctrl Pts',(-25.609673564302,26.0291498823676,-56.6107317605479));
#14893=CARTESIAN_POINT('Ctrl Pts',(-25.6054927483823,26.0326172744062,-56.6110641140929));
#14894=CARTESIAN_POINT('Ctrl Pts',(-25.5988833969117,26.0380706485203,-56.6115891093478));
#14895=CARTESIAN_POINT('Ctrl Pts',(-25.5964606796866,26.0400636930695,-56.6117814636095));
#14896=CARTESIAN_POINT('Ctrl Pts',(-25.591434921176,26.0441858355895,-56.6121803102211));
#14897=CARTESIAN_POINT('Ctrl Pts',(-25.5888314508093,26.046314402284,-56.6123868237642));
#14898=CARTESIAN_POINT('Ctrl Pts',(-25.5828985186458,26.0511496238528,-56.6128572156703));
#14899=CARTESIAN_POINT('Ctrl Pts',(-25.5795669784092,26.0538537079815,-56.6131211974846));
#14900=CARTESIAN_POINT('Ctrl Pts',(-25.5694281123333,26.0620495051353,-56.6139240974565));
#14901=CARTESIAN_POINT('Ctrl Pts',(-25.5626038632753,26.0675201331029,-56.6144638633773));
#14902=CARTESIAN_POINT('Ctrl Pts',(-25.5141004807907,26.1060793652963,-56.6182958067153));
#14903=CARTESIAN_POINT('Ctrl Pts',(-25.4716317730295,26.1381572506343,-56.6216280413161));
#14904=CARTESIAN_POINT('Ctrl Pts',(-25.4157979157781,26.1781981367017,-56.6259834511265));
#14905=CARTESIAN_POINT('Ctrl Pts',(-25.403140700652,26.187137645424,-56.6269691361736));
#14906=CARTESIAN_POINT('Ctrl Pts',(-25.3795328679331,26.2035574278932,-56.6288045874966));
#14907=CARTESIAN_POINT('Ctrl Pts',(-25.3685995515184,26.2110620942255,-56.629653441161));
#14908=CARTESIAN_POINT('Ctrl Pts',(-25.2371402059393,26.3001076136953,-56.6398457836409));
#14909=CARTESIAN_POINT('Ctrl Pts',(-25.1112853344877,26.3734529507193,-56.6494745816595));
#14910=CARTESIAN_POINT('Ctrl Pts',(-24.8875655462556,26.4842882380786,-56.6662597418593));
#14911=CARTESIAN_POINT('Ctrl Pts',(-24.792024652263,26.5259831846188,-56.6733292779252));
#14912=CARTESIAN_POINT('Ctrl Pts',(-24.5321834423552,26.6246837582465,-56.6921168627927));
#14913=CARTESIAN_POINT('Ctrl Pts',(-24.3649844631124,26.6731588156584,-56.7037648267124));
#14914=CARTESIAN_POINT('Ctrl Pts',(-24.1842849929204,26.710036194667,-56.7153746934155));
#14915=CARTESIAN_POINT('Ctrl Pts',(-24.1738868259481,26.7121048737872,-56.7160393513066));
#14916=CARTESIAN_POINT('Ctrl Pts',(-24.1602823429093,26.7147417149428,-56.7169043232264));
#14917=CARTESIAN_POINT('Ctrl Pts',(-24.1570852639833,26.7153563525372,-56.7171072591245));
#14918=CARTESIAN_POINT('Ctrl Pts',(-24.1518827444599,26.7163483631067,-56.7174369416389));
#14919=CARTESIAN_POINT('Ctrl Pts',(-24.1498778773046,26.7167286758579,-56.7175638569513));
#14920=CARTESIAN_POINT('Ctrl Pts',(-24.1460154594649,26.717457556374,-56.717808104599));
#14921=CARTESIAN_POINT('Ctrl Pts',(-24.1441579683827,26.7178063933908,-56.7179254519354));
#14922=CARTESIAN_POINT('Ctrl Pts',(-24.1398684058894,26.7186080678363,-56.7181961826111));
#14923=CARTESIAN_POINT('Ctrl Pts',(-24.1374361126518,26.7190597402282,-56.7183494987472));
#14924=CARTESIAN_POINT('Ctrl Pts',(-24.1296452435192,26.7204972121558,-56.7188399671293));
#14925=CARTESIAN_POINT('Ctrl Pts',(-24.1242846501612,26.7214722302502,-56.7191765035259));
#14926=CARTESIAN_POINT('Ctrl Pts',(-24.1056875644726,26.7248060836125,-56.7203408601092));
#14927=CARTESIAN_POINT('Ctrl Pts',(-24.0924385795353,26.7270957185495,-56.721164822986));
#14928=CARTESIAN_POINT('Ctrl Pts',(-23.7745517768539,26.7799849781797,-56.7408098903674));
#14929=CARTESIAN_POINT('Ctrl Pts',(-23.4641677781114,26.7866309711626,-56.7573672548889));
#14930=CARTESIAN_POINT('Ctrl Pts',(-23.0335314588877,26.7337610575943,-56.7818815932684));
#14931=CARTESIAN_POINT('Ctrl Pts',(-22.910525132612,26.7113396304774,-56.7890479320346));
#14932=CARTESIAN_POINT('Ctrl Pts',(-22.7466022986518,26.6714990820688,-56.79901929072));
#14933=CARTESIAN_POINT('Ctrl Pts',(-22.7042832530441,26.6602958482481,-56.8016317207004));
#14934=CARTESIAN_POINT('Ctrl Pts',(-22.6460937033803,26.6436156444302,-56.8052827378224));
#14935=CARTESIAN_POINT('Ctrl Pts',(-22.6300169632677,26.638871157604,-56.806297716353));
#14936=CARTESIAN_POINT('Ctrl Pts',(-22.6061190029991,26.6316153638276,-56.8078161192128));
#14937=CARTESIAN_POINT('Ctrl Pts',(-22.5982690172419,26.629199171296,-56.8083164406409));
#14938=CARTESIAN_POINT('Ctrl Pts',(-22.5840044327246,26.6247488250726,-56.8092284725018));
#14939=CARTESIAN_POINT('Ctrl Pts',(-22.5775867872259,26.622724532415,-56.8096398578396));
#14940=CARTESIAN_POINT('Ctrl Pts',(-22.5675134356821,26.6195124109695,-56.8102872681809));
#14941=CARTESIAN_POINT('Ctrl Pts',(-22.5638534090246,26.6183381087199,-56.8105228471339));
#14942=CARTESIAN_POINT('Ctrl Pts',(-22.5573228075707,26.6162299024264,-56.8109438210773));
#14943=CARTESIAN_POINT('Ctrl Pts',(-22.5544514227968,26.6152985062776,-56.8111291330943));
#14944=CARTESIAN_POINT('Ctrl Pts',(-22.5483688409357,26.6133160389131,-56.811522150884));
#14945=CARTESIAN_POINT('Ctrl Pts',(-22.5451579816624,26.6122639497693,-56.8117298901142));
#14946=CARTESIAN_POINT('Ctrl Pts',(-22.5360234233541,26.60925495047,-56.8123216698612));
#14947=CARTESIAN_POINT('Ctrl Pts',(-22.5301037678797,26.6072858944648,-56.812706111839));
#14948=CARTESIAN_POINT('Ctrl Pts',(-22.504980513387,26.5988480434532,-56.8143417209079));
#14949=CARTESIAN_POINT('Ctrl Pts',(-22.4858327670516,26.5922155033631,-56.8155983068113));
#14950=CARTESIAN_POINT('Ctrl Pts',(-22.45433637735,26.5809717629063,-56.817682184682));
#14951=CARTESIAN_POINT('Ctrl Pts',(-22.4419510186172,26.576464524197,-56.8185059764965));
#14952=CARTESIAN_POINT('Ctrl Pts',(-22.3082743265248,26.5268866462522,-56.8274448655465));
#14953=CARTESIAN_POINT('Ctrl Pts',(-22.1898796467717,26.4746650288207,-56.8357943590103));
#14954=CARTESIAN_POINT('Ctrl Pts',(-22.075035785626,26.4155366562829,-56.8443273945297));
#14955=CARTESIAN_POINT('',(-26.7730021430534,23.5518352458033,-56.6857734492205));
#14956=CARTESIAN_POINT('Ctrl Pts',(-22.0750360153845,26.415536774576,-57.0898644896988));
#14957=CARTESIAN_POINT('Ctrl Pts',(-22.1289579959314,26.4432989753045,-57.0862136761903));
#14958=CARTESIAN_POINT('Ctrl Pts',(-22.1836572224708,26.4695357137267,-57.082644257473));
#14959=CARTESIAN_POINT('Ctrl Pts',(-22.375909911966,26.5551613509025,-57.070447504258));
#14960=CARTESIAN_POINT('Ctrl Pts',(-22.5168434716501,26.6064968463387,-57.0621052936065));
#14961=CARTESIAN_POINT('Ctrl Pts',(-22.6781839966533,26.6528223466479,-57.0527257178279));
#14962=CARTESIAN_POINT('Ctrl Pts',(-22.6955643991644,26.6576551739239,-57.0517175734479));
#14963=CARTESIAN_POINT('Ctrl Pts',(-22.9490516746451,26.7258527058213,-57.0370375909288));
#14964=CARTESIAN_POINT('Ctrl Pts',(-23.1915375512655,26.7622888737644,-57.023206805814));
#14965=CARTESIAN_POINT('Ctrl Pts',(-23.4509605163593,26.7715083405287,-57.007458848676));
#14966=CARTESIAN_POINT('Ctrl Pts',(-23.4661309054112,26.7719401996617,-57.0065348529423));
#14967=CARTESIAN_POINT('Ctrl Pts',(-23.4868514514494,26.7723836057674,-57.0052684056177));
#14968=CARTESIAN_POINT('Ctrl Pts',(-23.492399593684,26.7724879967772,-57.0049288702612));
#14969=CARTESIAN_POINT('Ctrl Pts',(-23.5011881777624,26.7726306525099,-57.0043903346315));
#14970=CARTESIAN_POINT('Ctrl Pts',(-23.5044284730085,26.7726783601439,-57.0041916310542));
#14971=CARTESIAN_POINT('Ctrl Pts',(-23.5107014929228,26.7727612557337,-57.0038066622907));
#14972=CARTESIAN_POINT('Ctrl Pts',(-23.5137342074567,26.7727970500951,-57.0036204163386));
#14973=CARTESIAN_POINT('Ctrl Pts',(-23.5209393935235,26.772871918701,-57.0031776151157));
#14974=CARTESIAN_POINT('Ctrl Pts',(-23.5251118916147,26.7729071705807,-57.0029209401264));
#14975=CARTESIAN_POINT('Ctrl Pts',(-23.5374499685165,26.7729874472131,-57.0021612054212));
#14976=CARTESIAN_POINT('Ctrl Pts',(-23.5456156176842,26.7730095405904,-57.0016574266666));
#14977=CARTESIAN_POINT('Ctrl Pts',(-23.6100709692127,26.77293896674,-56.9976731049053));
#14978=CARTESIAN_POINT('Ctrl Pts',(-23.6663463484709,26.7714025875692,-56.9941474718841));
#14979=CARTESIAN_POINT('Ctrl Pts',(-23.8592825073757,26.7610728992429,-56.9818878262387));
#14980=CARTESIAN_POINT('Ctrl Pts',(-23.9953925163203,26.7450465956179,-56.9729339225174));
#14981=CARTESIAN_POINT('Ctrl Pts',(-24.1598872407253,26.7149614735939,-56.961778659204));
#14982=CARTESIAN_POINT('Ctrl Pts',(-24.1896384210411,26.7090850364896,-56.959747942694));
#14983=CARTESIAN_POINT('Ctrl Pts',(-24.2438547444788,26.697578941967,-56.9560252501412));
#14984=CARTESIAN_POINT('Ctrl Pts',(-24.26834575361,26.6920815632156,-56.9543353158208));
#14985=CARTESIAN_POINT('Ctrl Pts',(-24.3135640204857,26.681375297181,-56.9512011576024));
#14986=CARTESIAN_POINT('Ctrl Pts',(-24.3343086289694,26.6762452105117,-56.9497578190563));
#14987=CARTESIAN_POINT('Ctrl Pts',(-24.3729449782424,26.6662817543009,-56.9470603457249));
#14988=CARTESIAN_POINT('Ctrl Pts',(-24.3908490950885,26.6614996115543,-56.9458065844401));
#14989=CARTESIAN_POINT('Ctrl Pts',(-24.4244145439227,26.6522234820446,-56.9434497737337));
#14990=CARTESIAN_POINT('Ctrl Pts',(-24.440085022567,26.6477646201572,-56.9423468507494));
#14991=CARTESIAN_POINT('Ctrl Pts',(-24.5985362416258,26.6013774174911,-56.9311710076547));
#14992=CARTESIAN_POINT('Ctrl Pts',(-24.7382946168261,26.5497231748332,-56.9211084962021));
#14993=CARTESIAN_POINT('Ctrl Pts',(-24.8775252008891,26.48699900546,-56.9111586061001));
#14994=CARTESIAN_POINT('Ctrl Pts',(-24.8810567143021,26.4854003673905,-56.910906289081));
#14995=CARTESIAN_POINT('Ctrl Pts',(-24.8873795145018,26.4825244183001,-56.9104546548881));
#14996=CARTESIAN_POINT('Ctrl Pts',(-24.8901718715129,26.4812494863237,-56.910255237799));
#14997=CARTESIAN_POINT('Ctrl Pts',(-24.9404129271874,26.4582236656859,-56.9066680204525));
#14998=CARTESIAN_POINT('Ctrl Pts',(-24.9873316206943,26.4353255841775,-56.9033302150377));
#14999=CARTESIAN_POINT('Ctrl Pts',(-25.0387633769651,26.4086587061559,-56.8997017760999));
#15000=CARTESIAN_POINT('Ctrl Pts',(-25.043843217337,26.406007643684,-56.89934373574));
#15001=CARTESIAN_POINT('Ctrl Pts',(-25.0509506644732,26.4022742635281,-56.8988432836884));
#15002=CARTESIAN_POINT('Ctrl Pts',(-25.052984186301,26.4012033237815,-56.8987001560507));
#15003=CARTESIAN_POINT('Ctrl Pts',(-25.0567034270141,26.399239527328,-56.8984384881392));
#15004=CARTESIAN_POINT('Ctrl Pts',(-25.0583895010731,26.3983473480498,-56.8983199045851));
#15005=CARTESIAN_POINT('Ctrl Pts',(-25.0616212318466,26.3966336162769,-56.8980926923638));
#15006=CARTESIAN_POINT('Ctrl Pts',(-25.0631670106381,26.3958123019165,-56.8979840485186));
#15007=CARTESIAN_POINT('Ctrl Pts',(-25.0670947121816,26.3937213019853,-56.897708079418));
#15008=CARTESIAN_POINT('Ctrl Pts',(-25.0694757163648,26.392449879419,-56.8975408655051));
#15009=CARTESIAN_POINT('Ctrl Pts',(-25.0776803584006,26.3880554607897,-56.8969649362471));
#15010=CARTESIAN_POINT('Ctrl Pts',(-25.0834960369084,26.3849175182007,-56.8965571693341));
#15011=CARTESIAN_POINT('Ctrl Pts',(-25.0974369219202,26.3773400350551,-56.8955807279213));
#15012=CARTESIAN_POINT('Ctrl Pts',(-25.1055527821407,26.372883294793,-56.8950131199395));
#15013=CARTESIAN_POINT('Ctrl Pts',(-25.1350045167815,26.3565445868654,-56.8929559663072));
#15014=CARTESIAN_POINT('Ctrl Pts',(-25.156224968094,26.3444548448586,-56.891478824034));
#15015=CARTESIAN_POINT('Ctrl Pts',(-25.2500011312582,26.2896072869363,-56.8849645049247));
#15016=CARTESIAN_POINT('Ctrl Pts',(-25.3210072523645,26.2442532394234,-56.8800676114763));
#15017=CARTESIAN_POINT('Ctrl Pts',(-25.6303302846351,26.0291570664636,-56.8585238616396));
#15018=CARTESIAN_POINT('Ctrl Pts',(-25.8466414938083,25.8302310995459,-56.8427402297917));
#15019=CARTESIAN_POINT('Ctrl Pts',(-26.0956276621019,25.5293398477505,-56.8199987555657));
#15020=CARTESIAN_POINT('Ctrl Pts',(-26.1546221337973,25.4510358381957,-56.8141791980845));
#15021=CARTESIAN_POINT('Ctrl Pts',(-26.2152228800089,25.3624715188693,-56.8076472194698));
#15022=CARTESIAN_POINT('Ctrl Pts',(-26.2204582214526,25.354748634871,-56.8070780485343));
#15023=CARTESIAN_POINT('Ctrl Pts',(-26.2281804279205,25.343250073243,-56.8062311960031));
#15024=CARTESIAN_POINT('Ctrl Pts',(-26.2306930355567,25.339491673425,-56.8059544872497));
#15025=CARTESIAN_POINT('Ctrl Pts',(-26.2349802143327,25.3330495431564,-56.8054803432014));
#15026=CARTESIAN_POINT('Ctrl Pts',(-26.236758695394,25.3303684117129,-56.8052830554586));
#15027=CARTESIAN_POINT('Ctrl Pts',(-26.2402103890779,25.3251478909072,-56.804898995016));
#15028=CARTESIAN_POINT('Ctrl Pts',(-26.2418840283983,25.3226087872225,-56.8047122386739));
#15029=CARTESIAN_POINT('Ctrl Pts',(-26.2458777120233,25.316531205388,-56.804265311129));
#15030=CARTESIAN_POINT('Ctrl Pts',(-26.2481943819237,25.3129905265407,-56.804005013751));
#15031=CARTESIAN_POINT('Ctrl Pts',(-26.2551170602395,25.3023646457585,-56.803224052916));
#15032=CARTESIAN_POINT('Ctrl Pts',(-26.2597021529684,25.2952659200754,-56.8027026084648));
#15033=CARTESIAN_POINT('Ctrl Pts',(-26.2995268850307,25.2330731638249,-56.7981365016736));
#15034=CARTESIAN_POINT('Ctrl Pts',(-26.3331075729474,25.1769398266721,-56.7940307062087));
#15035=CARTESIAN_POINT('Ctrl Pts',(-26.4150117761055,25.0300617911736,-56.7833146009913));
#15036=CARTESIAN_POINT('Ctrl Pts',(-26.4607405198794,24.9379618357701,-56.7766188669879));
#15037=CARTESIAN_POINT('Ctrl Pts',(-26.6065914124831,24.6051566990373,-56.7525457358707));
#15038=CARTESIAN_POINT('Ctrl Pts',(-26.6818491650357,24.3546890214273,-56.7345563629171));
#15039=CARTESIAN_POINT('Ctrl Pts',(-26.7282239770885,24.0857588423779,-56.7165615523321));
#15040=CARTESIAN_POINT('Ctrl Pts',(-26.7302490556679,24.073599100837,-56.7157508905089));
#15041=CARTESIAN_POINT('Ctrl Pts',(-26.7352113916556,24.0427096739559,-56.7136995800862));
#15042=CARTESIAN_POINT('Ctrl Pts',(-26.7380532802513,24.0239648856954,-56.7124622354357));
#15043=CARTESIAN_POINT('Ctrl Pts',(-26.748141393568,23.9532178228717,-56.7078228969454));
#15044=CARTESIAN_POINT('Ctrl Pts',(-26.7542823736696,23.9010626919744,-56.7044650186804));
#15045=CARTESIAN_POINT('Ctrl Pts',(-26.7596780965245,23.8430631179638,-56.7008167489269));
#15046=CARTESIAN_POINT('Ctrl Pts',(-26.7601944196302,23.8373475906927,-56.7004581561174));
#15047=CARTESIAN_POINT('Ctrl Pts',(-26.7608962665517,23.8293397206702,-56.6999570635484));
#15048=CARTESIAN_POINT('Ctrl Pts',(-26.7610946038527,23.8270485558136,-56.6998138454095));
#15049=CARTESIAN_POINT('Ctrl Pts',(-26.7614530022426,23.8228561646309,-56.6995520634174));
#15050=CARTESIAN_POINT('Ctrl Pts',(-26.761613827664,23.8209550059082,-56.6994334561485));
#15051=CARTESIAN_POINT('Ctrl Pts',(-26.7619189709255,23.8173092857841,-56.6992062143715));
#15052=CARTESIAN_POINT('Ctrl Pts',(-26.7620635556231,23.8155647503987,-56.6990975646541));
#15053=CARTESIAN_POINT('Ctrl Pts',(-26.7623646150963,23.8118959027206,-56.6988692544573));
#15054=CARTESIAN_POINT('Ctrl Pts',(-26.7625207822942,23.8099715648311,-56.6987496114981));
#15055=CARTESIAN_POINT('Ctrl Pts',(-26.7628866824661,23.8054120192013,-56.6984663803339));
#15056=CARTESIAN_POINT('Ctrl Pts',(-26.7630949029009,23.8027766863175,-56.6983028774209));
#15057=CARTESIAN_POINT('Ctrl Pts',(-26.7636382385536,23.7957905193735,-56.6978699590247));
#15058=CARTESIAN_POINT('Ctrl Pts',(-26.7639677614759,23.7914392370389,-56.6976008551246));
#15059=CARTESIAN_POINT('Ctrl Pts',(-26.7700530152702,23.7088574988971,-56.692503554173));
#15060=CARTESIAN_POINT('Ctrl Pts',(-26.7729599694985,23.6304366978734,-56.687832280155));
#15061=CARTESIAN_POINT('Ctrl Pts',(-26.77300206773,23.5519818324221,-56.6832588369183));
#15062=CARTESIAN_POINT('Ctrl Pts',(-26.7730021430534,23.5518352458033,-56.6857734492205));
#15063=CARTESIAN_POINT('Ctrl Pts',(-26.7730504224152,23.4535279813412,-56.679673265777));
#15064=CARTESIAN_POINT('Ctrl Pts',(-26.7685963141078,23.3550373048322,-56.6735730823334));
#15065=CARTESIAN_POINT('Ctrl Pts',(-26.7596157733965,23.2568157492181,-56.6674728988899));
#15066=CARTESIAN_POINT('Ctrl Pts',(-26.7506466024252,23.1587185461992,-56.6613804385336));
#15067=CARTESIAN_POINT('Ctrl Pts',(-26.7371624241075,23.0608902267091,-56.6552879781773));
#15068=CARTESIAN_POINT('Ctrl Pts',(-26.719191208184,22.9637840950779,-56.649195517821));
#15069=CARTESIAN_POINT('Ctrl Pts',(-26.7012377562434,22.8667739498103,-56.6431090796705));
#15070=CARTESIAN_POINT('Ctrl Pts',(-26.6788061632909,22.7704850089876,-56.6370226415201));
#15071=CARTESIAN_POINT('Ctrl Pts',(-26.6519761626021,22.6753650646633,-56.6309362033697));
#15072=CARTESIAN_POINT('Ctrl Pts',(-26.6251605514189,22.5802961352085,-56.6248530295068));
#15073=CARTESIAN_POINT('Ctrl Pts',(-26.5939513369301,22.486395384793,-56.6187698556438));
#15074=CARTESIAN_POINT('Ctrl Pts',(-26.5584790597451,22.3940991169474,-56.6126866817809));
#15075=CARTESIAN_POINT('Ctrl Pts',(-26.5230158040352,22.3018263223192,-56.6066050550192));
#15076=CARTESIAN_POINT('Ctrl Pts',(-26.4832917988825,22.2111576150075,-56.6005234282574));
#15077=CARTESIAN_POINT('Ctrl Pts',(-26.439486663886,22.122511766752,-56.5944418014957));
#15078=CARTESIAN_POINT('Ctrl Pts',(-26.3956803167897,22.0338634656421,-56.5883600064537));
#15079=CARTESIAN_POINT('Ctrl Pts',(-26.3477928138976,21.9472385333444,-56.5822782114117));
#15080=CARTESIAN_POINT('Ctrl Pts',(-26.2960503898074,21.8630324260527,-56.5761964163697));
#15081=CARTESIAN_POINT('Ctrl Pts',(-26.2442576734751,21.7787444726934,-56.5701087099867));
#15082=CARTESIAN_POINT('Ctrl Pts',(-26.1886027854569,21.6968804204321,-56.5640210036038));
#15083=CARTESIAN_POINT('Ctrl Pts',(-26.1293559639129,21.6178076945985,-56.5579332972209));
#15084=CARTESIAN_POINT('Ctrl Pts',(-26.0700813385134,21.5386978608394,-56.551842733947));
#15085=CARTESIAN_POINT('Ctrl Pts',(-26.0072117069442,21.4623823051488,-56.5457521706732));
#15086=CARTESIAN_POINT('Ctrl Pts',(-25.941056938977,21.3891944925344,-56.5396616073993));
#15087=CARTESIAN_POINT('Ctrl Pts',(-25.8747881589441,21.3158805470054,-56.5335605475623));
#15088=CARTESIAN_POINT('Ctrl Pts',(-25.8052232455941,21.2457054299825,-56.5274594877253));
#15089=CARTESIAN_POINT('Ctrl Pts',(-25.7327082825262,21.1789650210451,-56.5213584278882));
#15090=CARTESIAN_POINT('Ctrl Pts',(-25.6620236823348,21.1139092184526,-56.5154113659706));
#15091=CARTESIAN_POINT('Ctrl Pts',(-25.5885365418587,21.0521169627958,-56.5094643040529));
#15092=CARTESIAN_POINT('Ctrl Pts',(-25.5125941137661,20.9938227795259,-56.5035172421352));
#15093=CARTESIAN_POINT('Ctrl Pts',(-25.4337781190522,20.9333228171747,-56.4973451508229));
#15094=CARTESIAN_POINT('Ctrl Pts',(-25.3520228255032,20.8763646210794,-56.4911730595105));
#15095=CARTESIAN_POINT('Ctrl Pts',(-25.2676801324481,20.8232468480425,-56.4850009681982));
#15096=CARTESIAN_POINT('Ctrl Pts',(-25.1834517154039,20.7702010443367,-56.4788372394594));
#15097=CARTESIAN_POINT('Ctrl Pts',(-25.0966432310861,20.7209855508462,-56.4726735107206));
#15098=CARTESIAN_POINT('Ctrl Pts',(-25.0076387365549,20.6758581585467,-56.4665097819818));
#15099=CARTESIAN_POINT('Ctrl Pts',(-24.9187285339321,20.630778574484,-56.4603525831351));
#15100=CARTESIAN_POINT('Ctrl Pts',(-24.8276273316299,20.5897786766317,-56.4541953842885));
#15101=CARTESIAN_POINT('Ctrl Pts',(-24.7347463655899,20.5530718698116,-56.4480381854418));
#15102=CARTESIAN_POINT('Ctrl Pts',(-24.6419332899036,20.5163918934413,-56.4418854871341));
#15103=CARTESIAN_POINT('Ctrl Pts',(-24.5473434396636,20.4839989284313,-56.4357327888264));
#15104=CARTESIAN_POINT('Ctrl Pts',(-24.4514099094734,20.4560591080417,-56.4295800905187));
#15105=CARTESIAN_POINT('Ctrl Pts',(-24.3555127574146,20.4281298824719,-56.4234297253229));
#15106=CARTESIAN_POINT('Ctrl Pts',(-24.2582733544368,20.4046505675488,-56.4172793601272));
#15107=CARTESIAN_POINT('Ctrl Pts',(-24.1601410627735,20.3857377913023,-56.4111289949314));
#15108=CARTESIAN_POINT('Ctrl Pts',(-24.0620197297389,20.3668271270831,-56.4049793165592));
#15109=CARTESIAN_POINT('Ctrl Pts',(-23.9630061328096,20.3524820698902,-56.398829638187));
#15110=CARTESIAN_POINT('Ctrl Pts',(-23.8635599713673,20.3427681574929,-56.3926799598148));
#15111=CARTESIAN_POINT('Ctrl Pts',(-23.7640983107092,20.3330527311304,-56.3865293229823));
#15112=CARTESIAN_POINT('Ctrl Pts',(-23.6642043840151,20.3279699254559,-56.3803786861499));
#15113=CARTESIAN_POINT('Ctrl Pts',(-23.5643421489165,20.3275333312074,-56.3742280493174));
#15114=CARTESIAN_POINT('Ctrl Pts',(-23.4643730822042,20.3270962698947,-56.3680708325956));
#15115=CARTESIAN_POINT('Ctrl Pts',(-23.3644362100354,20.3313153474497,-56.3619136158738));
#15116=CARTESIAN_POINT('Ctrl Pts',(-23.2649945056493,20.3401520003904,-56.355756399152));
#15117=CARTESIAN_POINT('Ctrl Pts',(-23.1654973231435,20.3489935832635,-56.3495957473441));
#15118=CARTESIAN_POINT('Ctrl Pts',(-23.0664962890278,20.3624578132963,-56.3434350955363));
#15119=CARTESIAN_POINT('Ctrl Pts',(-22.9684461885151,20.3804545978289,-56.3372744437285));
#15120=CARTESIAN_POINT('Ctrl Pts',(-22.8702320153172,20.3984814973818,-56.3311034829595));
#15121=CARTESIAN_POINT('Ctrl Pts',(-22.7729723775618,20.4210560031788,-56.3249325221905));
#15122=CARTESIAN_POINT('Ctrl Pts',(-22.6771090009775,20.4480375266909,-56.3187615614214));
#15123=CARTESIAN_POINT('Ctrl Pts',(-22.6039346857091,20.4686330301902,-56.314051151201));
#15124=CARTESIAN_POINT('Ctrl Pts',(-22.5315736407393,20.4917952623318,-56.3093407409807));
#15125=CARTESIAN_POINT('Ctrl Pts',(-22.4602141034591,20.5174429782486,-56.3046303307603));
#15126=CARTESIAN_POINT('Ctrl Pts',(-22.3667110836598,20.5510494025694,-56.298458239448));
#15127=CARTESIAN_POINT('Ctrl Pts',(-22.2745989956101,20.5890431831239,-56.2922861481356));
#15128=CARTESIAN_POINT('Ctrl Pts',(-22.1843193207942,20.6312896977649,-56.2861140568233));
#15129=CARTESIAN_POINT('Ctrl Pts',(-22.0941619660126,20.6734789725551,-56.2799503280845));
#15130=CARTESIAN_POINT('Ctrl Pts',(-22.0058324797428,20.7199093462814,-56.2737865993458));
#15131=CARTESIAN_POINT('Ctrl Pts',(-21.9197553449803,20.770397052246,-56.267622870607));
#15132=CARTESIAN_POINT('Ctrl Pts',(-21.8337694008637,20.8208312712245,-56.2614656717603));
#15133=CARTESIAN_POINT('Ctrl Pts',(-21.7500314369962,20.8753140583413,-56.2553084729137));
#15134=CARTESIAN_POINT('Ctrl Pts',(-21.6689432848947,20.9336147882519,-56.249151274067));
#15135=CARTESIAN_POINT('Ctrl Pts',(-21.5879144033147,20.9918729038647,-56.2429985757593));
#15136=CARTESIAN_POINT('Ctrl Pts',(-21.5095318343514,21.0539431611003,-56.2368458774516));
#15137=CARTESIAN_POINT('Ctrl Pts',(-21.4341694546978,21.119550992272,-56.2306931791439));
#15138=CARTESIAN_POINT('Ctrl Pts',(-21.3588356525657,21.1851339448608,-56.2245428139482));
#15139=CARTESIAN_POINT('Ctrl Pts',(-21.2865200913986,21.254251521018,-56.2183924487524));
#15140=CARTESIAN_POINT('Ctrl Pts',(-21.217563791652,21.3265887071514,-56.2122420835566));
#15141=CARTESIAN_POINT('Ctrl Pts',(-21.1486151923928,21.398917815247,-56.2060924051844));
#15142=CARTESIAN_POINT('Ctrl Pts',(-21.0830254084668,21.4744655040753,-56.1999427268122));
#15143=CARTESIAN_POINT('Ctrl Pts',(-21.0210980649029,21.5528804467762,-56.19379304844));
#15144=CARTESIAN_POINT('Ctrl Pts',(-20.9591610696316,21.6313076108649,-56.1876424116076));
#15145=CARTESIAN_POINT('Ctrl Pts',(-20.9008879177549,21.7126025754948,-56.1814917747751));
#15146=CARTESIAN_POINT('Ctrl Pts',(-20.8465408321569,21.7963823516964,-56.1753411379427));
#15147=CARTESIAN_POINT('Ctrl Pts',(-20.7921356065939,21.8802517546593,-56.1691839212209));
#15148=CARTESIAN_POINT('Ctrl Pts',(-20.7416650712976,21.9666109122583,-56.163026704499));
#15149=CARTESIAN_POINT('Ctrl Pts',(-20.6953470388263,22.0550494721425,-56.1568694877772));
#15150=CARTESIAN_POINT('Ctrl Pts',(-20.6490031657144,22.1435373715371,-56.1507088359694));
#15151=CARTESIAN_POINT('Ctrl Pts',(-20.6068165924558,22.2341065897243,-56.1445481841616));
#15152=CARTESIAN_POINT('Ctrl Pts',(-20.5689573532715,22.3263258093722,-56.1383875323538));
#15153=CARTESIAN_POINT('Ctrl Pts',(-20.5310347621173,22.418699344568,-56.1322165715848));
#15154=CARTESIAN_POINT('Ctrl Pts',(-20.4974541152694,22.5127279870423,-56.1260456108157));
#15155=CARTESIAN_POINT('Ctrl Pts',(-20.4683359047219,22.6079641114683,-56.1198746500467));
#15156=CARTESIAN_POINT('Ctrl Pts',(-20.44610942789,22.680659633388,-56.1151642398263));
#15157=CARTESIAN_POINT('Ctrl Pts',(-20.4264819900035,22.7540583630027,-56.1104538296058));
#15158=CARTESIAN_POINT('Ctrl Pts',(-20.4094869886824,22.8279580167423,-56.1057434193854));
#15159=CARTESIAN_POINT('Ctrl Pts',(-20.3872182912445,22.924789373139,-56.0995713280731));
#15160=CARTESIAN_POINT('Ctrl Pts',(-20.3693926077945,23.0228220673549,-56.0933992367608));
#15161=CARTESIAN_POINT('Ctrl Pts',(-20.3561353179195,23.1216119046324,-56.0872271454484));
#15162=CARTESIAN_POINT('Ctrl Pts',(-20.3428959903615,23.2202678914471,-56.0810634167097));
#15163=CARTESIAN_POINT('Ctrl Pts',(-20.3342128109161,23.3196785555821,-56.0748996879709));
#15164=CARTESIAN_POINT('Ctrl Pts',(-20.3301606246315,23.419387438681,-56.0687359592321));
#15165=CARTESIAN_POINT('Ctrl Pts',(-20.326112731258,23.5189906895761,-56.0625787603854));
#15166=CARTESIAN_POINT('Ctrl Pts',(-20.3266860948103,23.6188910996802,-56.0564215615387));
#15167=CARTESIAN_POINT('Ctrl Pts',(-20.3319038932866,23.7186259386206,-56.0502643626921));
#15168=CARTESIAN_POINT('Ctrl Pts',(-20.3371178778686,23.8182878774419,-56.0441116643844));
#15169=CARTESIAN_POINT('Ctrl Pts',(-20.3469695253134,23.9177840532136,-56.0379589660767));
#15170=CARTESIAN_POINT('Ctrl Pts',(-20.3614299334218,24.0166515017266,-56.031806267769));
#15171=CARTESIAN_POINT('Ctrl Pts',(-20.3758848581228,24.1154814595623,-56.0256559025732));
#15172=CARTESIAN_POINT('Ctrl Pts',(-20.3949450081306,24.2136827345155,-56.0195055373775));
#15173=CARTESIAN_POINT('Ctrl Pts',(-20.4185296932377,24.3107981421542,-56.0133551721817));
#15174=CARTESIAN_POINT('Ctrl Pts',(-20.4421117445961,24.407902704722,-56.0072054938095));
#15175=CARTESIAN_POINT('Ctrl Pts',(-20.4702172240049,24.5039212189263,-56.0010558154373));
#15176=CARTESIAN_POINT('Ctrl Pts',(-20.5027146764818,24.5984083328743,-55.994906137065));
#15177=CARTESIAN_POINT('Ctrl Pts',(-20.5352171938604,24.692910173144,-55.9887555002326));
#15178=CARTESIAN_POINT('Ctrl Pts',(-20.5721129026271,24.7858797282602,-55.9826048634001));
#15179=CARTESIAN_POINT('Ctrl Pts',(-20.6132213303213,24.8768893639367,-55.9764542265677));
#15180=CARTESIAN_POINT('Ctrl Pts',(-20.6543737353976,24.967996360805,-55.9702970098458));
#15181=CARTESIAN_POINT('Ctrl Pts',(-20.6997476797155,25.0571388546636,-55.964139793124));
#15182=CARTESIAN_POINT('Ctrl Pts',(-20.7491156638787,25.1439117833112,-55.9579825764022));
#15183=CARTESIAN_POINT('Ctrl Pts',(-20.798511190238,25.2307331222204,-55.9518219245944));
#15184=CARTESIAN_POINT('Ctrl Pts',(-20.8519049618298,25.3151818960516,-55.9456612727866));
#15185=CARTESIAN_POINT('Ctrl Pts',(-20.9090260148504,25.3968819068589,-55.9395006209787));
#15186=CARTESIAN_POINT('Ctrl Pts',(-20.9662426517051,25.478718630837,-55.9333296602097));
#15187=CARTESIAN_POINT('Ctrl Pts',(-21.0271987630487,25.5577970598691,-55.9271586994407));
#15188=CARTESIAN_POINT('Ctrl Pts',(-21.0915828852142,25.6337738615533,-55.9209877386716));
#15189=CARTESIAN_POINT('Ctrl Pts',(-21.1407284945332,25.691768380812,-55.9162773284513));
#15190=CARTESIAN_POINT('Ctrl Pts',(-21.1918706150156,25.7479563985689,-55.9115669182309));
#15191=CARTESIAN_POINT('Ctrl Pts',(-21.2448571149293,25.8022004740009,-55.9068565080105));
#15192=CARTESIAN_POINT('Ctrl Pts',(-21.3142739181782,25.8732648077051,-55.900685471614));
#15193=CARTESIAN_POINT('Ctrl Pts',(-21.3871018969899,25.9412415898445,-55.8945144352176));
#15194=CARTESIAN_POINT('Ctrl Pts',(-21.4630352761606,26.0057854047592,-55.8883433988211));
#15195=CARTESIAN_POINT('Ctrl Pts',(-21.5388783893179,26.0702524930363,-55.8821796982611));
#15196=CARTESIAN_POINT('Ctrl Pts',(-21.6178192436625,26.1312944400473,-55.8760159977011));
#15197=CARTESIAN_POINT('Ctrl Pts',(-21.6995142811262,26.1886015401434,-55.8698522971412));
#15198=CARTESIAN_POINT('Ctrl Pts',(-21.7811175908716,26.2458442954555,-55.8636955172242));
#15199=CARTESIAN_POINT('Ctrl Pts',(-21.8654685800901,26.2993602956288,-55.8575387373072));
#15200=CARTESIAN_POINT('Ctrl Pts',(-21.9521905582162,26.3488799616005,-55.8513819573902));
#15201=CARTESIAN_POINT('Ctrl Pts',(-21.9926372384212,26.3719756766279,-55.8485104672123));
#15202=CARTESIAN_POINT('Ctrl Pts',(-22.0335992091366,26.3942026744379,-55.8456389770345));
#15203=CARTESIAN_POINT('Ctrl Pts',(-22.0750360153461,26.4155367745563,-55.8427674868566));
#15204=CARTESIAN_POINT('Origin',(-23.5502525316942,23.5502525316942,-77.3107734492734));
#15205=CARTESIAN_POINT('',(-22.0750359442814,26.415536737968,-54.34883718749));
#15206=CARTESIAN_POINT('',(-22.0750360179885,26.4155367759168,-54.5955012513333));
#15207=CARTESIAN_POINT('',(-22.0750360153461,26.4155367745563,-77.3107734492734));
#15208=CARTESIAN_POINT('Ctrl Pts',(-22.0750359442814,26.415536737968,-54.34883718749));
#15209=CARTESIAN_POINT('Ctrl Pts',(-21.9634080683998,26.3580641515636,-54.3561191662865));
#15210=CARTESIAN_POINT('Ctrl Pts',(-21.8551854385235,26.2940922482147,-54.3631623810082));
#15211=CARTESIAN_POINT('Ctrl Pts',(-21.6005988914945,26.1227617454723,-54.3803202095482));
#15212=CARTESIAN_POINT('Ctrl Pts',(-21.4590714163177,26.0090956425743,-54.3903947990664));
#15213=CARTESIAN_POINT('Ctrl Pts',(-21.2709694206182,25.8299796957877,-54.4054241972002));
#15214=CARTESIAN_POINT('Ctrl Pts',(-21.216088097284,25.7737548164187,-54.4100375124971));
#15215=CARTESIAN_POINT('Ctrl Pts',(-21.1365410134935,25.6860667975991,-54.4171248047951));
#15216=CARTESIAN_POINT('Ctrl Pts',(-21.1103146136579,25.6560560861961,-54.4195324404199));
#15217=CARTESIAN_POINT('Ctrl Pts',(-21.0798485180739,25.6198605189877,-54.422418471595));
#15218=CARTESIAN_POINT('Ctrl Pts',(-21.0750645639555,25.6141366695434,-54.4228743400978));
#15219=CARTESIAN_POINT('Ctrl Pts',(-21.0677310852834,25.6053002242018,-54.4235773326841));
#15220=CARTESIAN_POINT('Ctrl Pts',(-21.0651674223618,25.6021993510616,-54.4238238799014));
#15221=CARTESIAN_POINT('Ctrl Pts',(-21.060505101604,25.5965384977159,-54.4242737067586));
#15222=CARTESIAN_POINT('Ctrl Pts',(-21.0584045654735,25.593980065758,-54.4244769096891));
#15223=CARTESIAN_POINT('Ctrl Pts',(-21.0541595360249,25.5887933887831,-54.4248886665072));
#15224=CARTESIAN_POINT('Ctrl Pts',(-21.0520152433715,25.586164985643,-54.4250972281569));
#15225=CARTESIAN_POINT('Ctrl Pts',(-21.0458974877022,25.578641824525,-54.4256939015152));
#15226=CARTESIAN_POINT('Ctrl Pts',(-21.0419342490145,25.5737388058037,-54.4260824254543));
#15227=CARTESIAN_POINT('Ctrl Pts',(-21.0249478608852,25.5525979446066,-54.4277562289903));
#15228=CARTESIAN_POINT('Ctrl Pts',(-21.0120680400948,25.5362460580891,-54.4290472450986));
#15229=CARTESIAN_POINT('Ctrl Pts',(-20.7814081133303,25.2374971202017,-54.452572927402));
#15230=CARTESIAN_POINT('Ctrl Pts',(-20.6118750318638,24.9210523774672,-54.4769229566944));
#15231=CARTESIAN_POINT('Ctrl Pts',(-20.4682295873338,24.4966403678763,-54.5070118918893));
#15232=CARTESIAN_POINT('Ctrl Pts',(-20.442564008967,24.4086172455943,-54.5131005701901));
#15233=CARTESIAN_POINT('Ctrl Pts',(-20.4127760401292,24.2874472422953,-54.5211790219131));
#15234=CARTESIAN_POINT('Ctrl Pts',(-20.4053643899234,24.2551592969902,-54.523302784798));
#15235=CARTESIAN_POINT('Ctrl Pts',(-20.3960356918904,24.2114391321839,-54.5261344938964));
#15236=CARTESIAN_POINT('Ctrl Pts',(-20.3936808071156,24.2001037070915,-54.5268647058411));
#15237=CARTESIAN_POINT('Ctrl Pts',(-20.3903291676397,24.183522145934,-54.5279268240371));
#15238=CARTESIAN_POINT('Ctrl Pts',(-20.3892843172612,24.178285985677,-54.5282613433917));
#15239=CARTESIAN_POINT('Ctrl Pts',(-20.3876645171647,24.1700620746803,-54.528785334741));
#15240=CARTESIAN_POINT('Ctrl Pts',(-20.3870807830107,24.1670760945827,-54.5289752978534));
#15241=CARTESIAN_POINT('Ctrl Pts',(-20.3861029735488,24.1620364062077,-54.5292954194609));
#15242=CARTESIAN_POINT('Ctrl Pts',(-20.3857066685261,24.1599831405626,-54.529425704586));
#15243=CARTESIAN_POINT('Ctrl Pts',(-20.3849341154542,24.1559594825258,-54.5296807429276));
#15244=CARTESIAN_POINT('Ctrl Pts',(-20.3845577081447,24.1539891221694,-54.5298055052476));
#15245=CARTESIAN_POINT('Ctrl Pts',(-20.383839674244,24.1502113320759,-54.5300444654509));
#15246=CARTESIAN_POINT('Ctrl Pts',(-20.3834977563847,24.1484039665742,-54.5301586796248));
#15247=CARTESIAN_POINT('Ctrl Pts',(-20.3827074676054,24.1442068576727,-54.5304236594829));
#15248=CARTESIAN_POINT('Ctrl Pts',(-20.3822602525221,24.1418168930123,-54.5305743584375));
#15249=CARTESIAN_POINT('Ctrl Pts',(-20.3808608987448,24.1342915017538,-54.5310482833016));
#15250=CARTESIAN_POINT('Ctrl Pts',(-20.3799185329231,24.1291542320742,-54.5313709505443));
#15251=CARTESIAN_POINT('Ctrl Pts',(-20.3723412663951,24.0872736149722,-54.5339945847663));
#15252=CARTESIAN_POINT('Ctrl Pts',(-20.3663325306277,24.0504178800987,-54.5362604995031));
#15253=CARTESIAN_POINT('Ctrl Pts',(-20.3598623774903,24.0058698233629,-54.5389567647833));
#15254=CARTESIAN_POINT('Ctrl Pts',(-20.3587865005749,23.9982715345961,-54.5394151623451));
#15255=CARTESIAN_POINT('Ctrl Pts',(-20.3563798038378,23.9808257568182,-54.5404643852637));
#15256=CARTESIAN_POINT('Ctrl Pts',(-20.3550673622209,23.970975767673,-54.5410543989947));
#15257=CARTESIAN_POINT('Ctrl Pts',(-20.3533295086966,23.9574556687838,-54.5418611761408));
#15258=CARTESIAN_POINT('Ctrl Pts',(-20.3528648313952,23.9537907628808,-54.5420795602604));
#15259=CARTESIAN_POINT('Ctrl Pts',(-20.3483996903152,23.9180822978199,-54.5442044068596));
#15260=CARTESIAN_POINT('Ctrl Pts',(-20.3448746309769,23.8859801009238,-54.5460915612406));
#15261=CARTESIAN_POINT('Ctrl Pts',(-20.313684050082,23.5563354280417,-54.5652821737521));
#15262=CARTESIAN_POINT('Ctrl Pts',(-20.3270446235538,23.2563618601901,-54.5813170389239));
#15263=CARTESIAN_POINT('Ctrl Pts',(-20.3965878448685,22.8814366968608,-54.6033231574784));
#15264=CARTESIAN_POINT('Ctrl Pts',(-20.4147290828368,22.8009817787368,-54.6081543329074));
#15265=CARTESIAN_POINT('Ctrl Pts',(-20.4469014448502,22.6801101628351,-54.6156313883517));
#15266=CARTESIAN_POINT('Ctrl Pts',(-20.4586852539192,22.6391283844278,-54.6182052580888));
#15267=CARTESIAN_POINT('Ctrl Pts',(-20.4735236451243,22.5911306848696,-54.6212695649207));
#15268=CARTESIAN_POINT('Ctrl Pts',(-20.4757947286929,22.5838754963129,-54.6217341055924));
#15269=CARTESIAN_POINT('Ctrl Pts',(-20.4793161907327,22.5727639195181,-54.6224476603139));
#15270=CARTESIAN_POINT('Ctrl Pts',(-20.4805482207853,22.5689017073094,-54.6226960697375));
#15271=CARTESIAN_POINT('Ctrl Pts',(-20.4828094830234,22.561858945672,-54.6231497593548));
#15272=CARTESIAN_POINT('Ctrl Pts',(-20.4838363842109,22.5586776489706,-54.6233549624022));
#15273=CARTESIAN_POINT('Ctrl Pts',(-20.4859120022386,22.5522815316441,-54.6237680690346));
#15274=CARTESIAN_POINT('Ctrl Pts',(-20.4869608327213,22.5490667525951,-54.6239759761574));
#15275=CARTESIAN_POINT('Ctrl Pts',(-20.4899632202671,22.5399129943118,-54.6245687546988));
#15276=CARTESIAN_POINT('Ctrl Pts',(-20.4919289945143,22.5339780650848,-54.6249540297664));
#15277=CARTESIAN_POINT('Ctrl Pts',(-20.5003747544217,22.5087256417164,-54.6265973726622));
#15278=CARTESIAN_POINT('Ctrl Pts',(-20.5070204782076,22.4894644488189,-54.6278609228495));
#15279=CARTESIAN_POINT('Ctrl Pts',(-20.636204621896,22.1262599378502,-54.6518830474312));
#15280=CARTESIAN_POINT('Ctrl Pts',(-20.8161184110933,21.8056060612468,-54.6768763257385));
#15281=CARTESIAN_POINT('Ctrl Pts',(-21.127257077375,21.4214095583183,-54.7100126527375));
#15282=CARTESIAN_POINT('Ctrl Pts',(-21.2147374262675,21.3257846333039,-54.7185446932962));
#15283=CARTESIAN_POINT('Ctrl Pts',(-21.3112385772449,21.2322883971883,-54.7269739522954));
#15284=CARTESIAN_POINT('Ctrl Pts',(-21.3147392972331,21.2289120145895,-54.7272784742693));
#15285=CARTESIAN_POINT('Ctrl Pts',(-21.3203030766058,21.2235701061391,-54.7277604419814));
#15286=CARTESIAN_POINT('Ctrl Pts',(-21.3223611049412,21.2215993861215,-54.7279382851833));
#15287=CARTESIAN_POINT('Ctrl Pts',(-21.32626432619,21.2178716631422,-54.7282747509249));
#15288=CARTESIAN_POINT('Ctrl Pts',(-21.3281089925562,21.2161141155363,-54.7284334156561));
#15289=CARTESIAN_POINT('Ctrl Pts',(-21.3313110277448,21.2130705403174,-54.7287082231869));
#15290=CARTESIAN_POINT('Ctrl Pts',(-21.3326674332857,21.2117835047129,-54.7288244449558));
#15291=CARTESIAN_POINT('Ctrl Pts',(-21.3353037893955,21.2092863349823,-54.7290499701177));
#15292=CARTESIAN_POINT('Ctrl Pts',(-21.3365836096756,21.208076071885,-54.7291592837957));
#15293=CARTESIAN_POINT('Ctrl Pts',(-21.3396148324195,21.2052142974818,-54.7294177960252));
#15294=CARTESIAN_POINT('Ctrl Pts',(-21.3413670973102,21.2035636952212,-54.7295669235955));
#15295=CARTESIAN_POINT('Ctrl Pts',(-21.3474927006835,21.1978064260285,-54.7300871685351));
#15296=CARTESIAN_POINT('Ctrl Pts',(-21.3518756902447,21.1937099758455,-54.7304574983622));
#15297=CARTESIAN_POINT('Ctrl Pts',(-21.4058921103276,21.1435067519798,-54.7349983775873));
#15298=CARTESIAN_POINT('Ctrl Pts',(-21.4569603154764,21.098959778807,-54.7390524286924));
#15299=CARTESIAN_POINT('Ctrl Pts',(-21.5209131961418,21.0466310039921,-54.7439003135547));
#15300=CARTESIAN_POINT('Ctrl Pts',(-21.5324924332075,21.037289521517,-54.7447692460259));
#15301=CARTESIAN_POINT('Ctrl Pts',(-21.6955988640664,20.907558587243,-54.7568927481815));
#15302=CARTESIAN_POINT('Ctrl Pts',(-21.8576167316477,20.8009676455572,-54.7675575124803));
#15303=CARTESIAN_POINT('Ctrl Pts',(-22.1279887555187,20.6561046954278,-54.7847432974721));
#15304=CARTESIAN_POINT('Ctrl Pts',(-22.2304877550098,20.6079499299511,-54.7911290819701));
#15305=CARTESIAN_POINT('Ctrl Pts',(-22.4113832564205,20.5343212314807,-54.8024054318773));
#15306=CARTESIAN_POINT('Ctrl Pts',(-22.4886152769386,20.5062765845659,-54.8072208502105));
#15307=CARTESIAN_POINT('Ctrl Pts',(-22.6066365938036,20.4684586068987,-54.8146324315996));
#15308=CARTESIAN_POINT('Ctrl Pts',(-22.6466861380622,20.4564793733931,-54.8171562465747));
#15309=CARTESIAN_POINT('Ctrl Pts',(-22.6942402668426,20.4432575642188,-54.8201669187194));
#15310=CARTESIAN_POINT('Ctrl Pts',(-22.701531628638,20.4412579108123,-54.8206289195138));
#15311=CARTESIAN_POINT('Ctrl Pts',(-22.7127346515487,20.4382278329951,-54.8213393821206));
#15312=CARTESIAN_POINT('Ctrl Pts',(-22.7166413629431,20.4371790754502,-54.8215872474989));
#15313=CARTESIAN_POINT('Ctrl Pts',(-22.7234663050792,20.4353606866391,-54.8220204645779));
#15314=CARTESIAN_POINT('Ctrl Pts',(-22.7263836679501,20.434587792643,-54.8222057100522));
#15315=CARTESIAN_POINT('Ctrl Pts',(-22.7329579988879,20.4328559412376,-54.822623310694));
#15316=CARTESIAN_POINT('Ctrl Pts',(-22.7366155726289,20.4318993197898,-54.8228557413549));
#15317=CARTESIAN_POINT('Ctrl Pts',(-22.746427142136,20.4293515866171,-54.8234795226929));
#15318=CARTESIAN_POINT('Ctrl Pts',(-22.7525841527638,20.427772247976,-54.823871254363));
#15319=CARTESIAN_POINT('Ctrl Pts',(-22.7793516980797,20.420990425734,-54.8255756081299));
#15320=CARTESIAN_POINT('Ctrl Pts',(-22.8000083744637,20.4159738119994,-54.8268942278418));
#15321=CARTESIAN_POINT('Ctrl Pts',(-22.833501515297,20.4081898447627,-54.8290380683351));
#15322=CARTESIAN_POINT('Ctrl Pts',(-22.8463081423857,20.4052958965979,-54.8298591639152));
#15323=CARTESIAN_POINT('Ctrl Pts',(-22.8650067500868,20.4011904557137,-54.8310600734351));
#15324=CARTESIAN_POINT('Ctrl Pts',(-22.8708851226519,20.3999170476021,-54.8314379037886));
#15325=CARTESIAN_POINT('Ctrl Pts',(-22.8797380823231,20.3980251975436,-54.8320073730602));
#15326=CARTESIAN_POINT('Ctrl Pts',(-22.8827100591102,20.3973944885567,-54.8321986223099));
#15327=CARTESIAN_POINT('Ctrl Pts',(-22.8893202399611,20.3960014500662,-54.8326241628575));
#15328=CARTESIAN_POINT('Ctrl Pts',(-22.8929588759452,20.3952412115666,-54.8328585198933));
#15329=CARTESIAN_POINT('Ctrl Pts',(-22.9034154196993,20.3930753474378,-54.8335323344072));
#15330=CARTESIAN_POINT('Ctrl Pts',(-22.9102365460895,20.391685521293,-54.8339722873282));
#15331=CARTESIAN_POINT('Ctrl Pts',(-22.9231752579306,20.3890928510203,-54.8348075866252));
#15332=CARTESIAN_POINT('Ctrl Pts',(-22.9292919437922,20.3878856362517,-54.8352027945176));
#15333=CARTESIAN_POINT('Ctrl Pts',(-22.9394200686109,20.3859172246424,-54.8358577303089));
#15334=CARTESIAN_POINT('Ctrl Pts',(-22.9434295390428,20.3851458843982,-54.8361171435987));
#15335=CARTESIAN_POINT('Ctrl Pts',(-22.9529699124465,20.383329305798,-54.8367347428039));
#15336=CARTESIAN_POINT('Ctrl Pts',(-22.9585020959488,20.3822909367354,-54.8370931386916));
#15337=CARTESIAN_POINT('Ctrl Pts',(-22.9844354367949,20.3774936510289,-54.8387744604907));
#15338=CARTESIAN_POINT('Ctrl Pts',(-23.0048695065764,20.3739173440357,-54.840102910461));
#15339=CARTESIAN_POINT('Ctrl Pts',(-23.3240678213129,20.3212231781401,-54.8609117696472));
#15340=CARTESIAN_POINT('Ctrl Pts',(-23.6282327343412,20.3142601291747,-54.8817312681102));
#15341=CARTESIAN_POINT('Ctrl Pts',(-23.9965121896926,20.3578212144398,-54.9065290676153));
#15342=CARTESIAN_POINT('Ctrl Pts',(-24.0639483670755,20.3679761280843,-54.9110428536091));
#15343=CARTESIAN_POINT('Ctrl Pts',(-24.1802454107345,20.3892825100537,-54.9187275141719));
#15344=CARTESIAN_POINT('Ctrl Pts',(-24.2292620805534,20.399447996854,-54.9219352049622));
#15345=CARTESIAN_POINT('Ctrl Pts',(-24.283942889799,20.4121236430962,-54.9254635358839));
#15346=CARTESIAN_POINT('Ctrl Pts',(-24.2898567194452,20.4135121678934,-54.9258444699291));
#15347=CARTESIAN_POINT('Ctrl Pts',(-24.2990113188923,20.4156889314076,-54.9264330921904));
#15348=CARTESIAN_POINT('Ctrl Pts',(-24.3022548118121,20.4164654845921,-54.9266414352341));
#15349=CARTESIAN_POINT('Ctrl Pts',(-24.307648497744,20.4177656904545,-54.9269875428781));
#15350=CARTESIAN_POINT('Ctrl Pts',(-24.3097993576234,20.4182865230635,-54.9271254684937));
#15351=CARTESIAN_POINT('Ctrl Pts',(-24.3139819178319,20.4193038956468,-54.9273934952788));
#15352=CARTESIAN_POINT('Ctrl Pts',(-24.3160136739178,20.419800198574,-54.9275236100879));
#15353=CARTESIAN_POINT('Ctrl Pts',(-24.3198169282496,20.420733154714,-54.9277670131379));
#15354=CARTESIAN_POINT('Ctrl Pts',(-24.3215885268806,20.4211693314751,-54.9278803279453));
#15355=CARTESIAN_POINT('Ctrl Pts',(-24.3256135252938,20.4221639329359,-54.9281376274386));
#15356=CARTESIAN_POINT('Ctrl Pts',(-24.3278666884065,20.4227232871546,-54.9282815571528));
#15357=CARTESIAN_POINT('Ctrl Pts',(-24.333587522705,20.4241500651316,-54.9286467370445));
#15358=CARTESIAN_POINT('Ctrl Pts',(-24.3370543690444,20.4250208269056,-54.9288677936444));
#15359=CARTESIAN_POINT('Ctrl Pts',(-24.356094056155,20.4298366817899,-54.9300805180366));
#15360=CARTESIAN_POINT('Ctrl Pts',(-24.3716390417828,20.4338924971086,-54.9310658546786));
#15361=CARTESIAN_POINT('Ctrl Pts',(-24.6845075584583,20.5180262119252,-54.9508125533594));
#15362=CARTESIAN_POINT('Ctrl Pts',(-24.9689232365307,20.6402047948141,-54.9673273060959));
#15363=CARTESIAN_POINT('Ctrl Pts',(-25.295285764587,20.8398041747061,-54.9889391325971));
#15364=CARTESIAN_POINT('Ctrl Pts',(-25.3574912261611,20.8808783091154,-54.9931865587937));
#15365=CARTESIAN_POINT('Ctrl Pts',(-25.4823553521446,20.9696921958522,-55.0020520247273));
#15366=CARTESIAN_POINT('Ctrl Pts',(-25.5447988174219,21.0176458437683,-55.006674515143));
#15367=CARTESIAN_POINT('Ctrl Pts',(-25.6361753409885,21.0932955346298,-55.0137755930199));
#15368=CARTESIAN_POINT('Ctrl Pts',(-25.6664526318269,21.1193250195556,-55.0161875546358));
#15369=CARTESIAN_POINT('Ctrl Pts',(-25.7018058531225,21.1508793689383,-55.0190782309406));
#15370=CARTESIAN_POINT('Ctrl Pts',(-25.7073568406882,21.1558686301982,-55.0195343339643));
#15371=CARTESIAN_POINT('Ctrl Pts',(-25.715874020412,21.1635775800833,-55.020237612344));
#15372=CARTESIAN_POINT('Ctrl Pts',(-25.718852559336,21.1662836399253,-55.0204842100909));
#15373=CARTESIAN_POINT('Ctrl Pts',(-25.7242719577914,21.1712258282852,-55.0209340892659));
#15374=CARTESIAN_POINT('Ctrl Pts',(-25.7267144588198,21.173460155355,-55.02113729389));
#15375=CARTESIAN_POINT('Ctrl Pts',(-25.7316524626707,21.1779912883834,-55.0215490189667));
#15376=CARTESIAN_POINT('Ctrl Pts',(-25.7341477905415,21.180288278035,-55.0217575471256));
#15377=CARTESIAN_POINT('Ctrl Pts',(-25.7412692685266,21.1868645113543,-55.02235402115));
#15378=CARTESIAN_POINT('Ctrl Pts',(-25.7458864802154,21.1911533733365,-55.0227423788047));
#15379=CARTESIAN_POINT('Ctrl Pts',(-25.7656836733363,21.2096511676624,-55.0244146116046));
#15380=CARTESIAN_POINT('Ctrl Pts',(-25.7807382601546,21.2239930295828,-55.0257042100048));
#15381=CARTESIAN_POINT('Ctrl Pts',(-26.0444468928259,21.4801303568751,-55.0486183487306));
#15382=CARTESIAN_POINT('Ctrl Pts',(-26.2525510821041,21.7603180086611,-55.0722270704238));
#15383=CARTESIAN_POINT('Ctrl Pts',(-26.4577859842493,22.1565916928722,-55.1022570871738));
#15384=CARTESIAN_POINT('Ctrl Pts',(-26.4994772107453,22.2471338850914,-55.1088943426205));
#15385=CARTESIAN_POINT('Ctrl Pts',(-26.5498173979832,22.3713086871535,-55.1175781841747));
#15386=CARTESIAN_POINT('Ctrl Pts',(-26.5622159571699,22.4033547524672,-55.1197827489849));
#15387=CARTESIAN_POINT('Ctrl Pts',(-26.5803555802647,22.4525639721244,-55.1231061545352));
#15388=CARTESIAN_POINT('Ctrl Pts',(-26.5864681647991,22.4695863832581,-55.1242446172016));
#15389=CARTESIAN_POINT('Ctrl Pts',(-26.5937279776328,22.4903515611689,-55.125619075039));
#15390=CARTESIAN_POINT('Ctrl Pts',(-26.5950119530271,22.4940456750877,-55.1258630413849));
#15391=CARTESIAN_POINT('Ctrl Pts',(-26.597003331298,22.4998088592817,-55.1262427875031));
#15392=CARTESIAN_POINT('Ctrl Pts',(-26.597715352722,22.5018763118572,-55.1263788420695));
#15393=CARTESIAN_POINT('Ctrl Pts',(-26.5989698109654,22.5055308813404,-55.1266190329537));
#15394=CARTESIAN_POINT('Ctrl Pts',(-26.5995131101697,22.5071176889107,-55.1267232206084));
#15395=CARTESIAN_POINT('Ctrl Pts',(-26.6006708534005,22.5105077292374,-55.1269455867946));
#15396=CARTESIAN_POINT('Ctrl Pts',(-26.6012849355981,22.512311077655,-55.1270637433277));
#15397=CARTESIAN_POINT('Ctrl Pts',(-26.6030528620615,22.517517996102,-55.1274045252061));
#15398=CARTESIAN_POINT('Ctrl Pts',(-26.6042026173207,22.5209229669302,-55.1276269066011));
#15399=CARTESIAN_POINT('Ctrl Pts',(-26.6092677257412,22.5360063486839,-55.128609978525));
#15400=CARTESIAN_POINT('Ctrl Pts',(-26.6131218719575,22.5477054289738,-55.1293670772155));
#15401=CARTESIAN_POINT('Ctrl Pts',(-26.6178227146822,22.5622547741731,-55.1303022743309));
#15402=CARTESIAN_POINT('Ctrl Pts',(-26.6187325982724,22.5650842833267,-55.1304838509068));
#15403=CARTESIAN_POINT('Ctrl Pts',(-26.6222418452067,22.5760491847498,-55.1311863584215));
#15404=CARTESIAN_POINT('Ctrl Pts',(-26.6248128076308,22.5841937256383,-55.1317057458969));
#15405=CARTESIAN_POINT('Ctrl Pts',(-26.6289021989864,22.5973301787154,-55.132539719737));
#15406=CARTESIAN_POINT('Ctrl Pts',(-26.6304409147866,22.6023156613576,-55.1328553568212));
#15407=CARTESIAN_POINT('Ctrl Pts',(-26.6332670492646,22.6115519547058,-55.1334385489814));
#15408=CARTESIAN_POINT('Ctrl Pts',(-26.6345577979947,22.6158017231831,-55.1337062714734));
#15409=CARTESIAN_POINT('Ctrl Pts',(-26.7265388096929,22.9209145330444,-55.1528843487594));
#15410=CARTESIAN_POINT('Ctrl Pts',(-26.7727633327215,23.2334680455744,-55.1696604153421));
#15411=CARTESIAN_POINT('Ctrl Pts',(-26.7730574974556,23.6215446029327,-55.1917202091736));
#15412=CARTESIAN_POINT('Ctrl Pts',(-26.770582859349,23.695256143819,-55.1959563771899));
#15413=CARTESIAN_POINT('Ctrl Pts',(-26.7593379903672,23.8606823936348,-55.2056358162423));
#15414=CARTESIAN_POINT('Ctrl Pts',(-26.7491595350554,23.9522322375907,-55.2111131797558));
#15415=CARTESIAN_POINT('Ctrl Pts',(-26.7335159642199,24.0532988590675,-55.217338916616));
#15416=CARTESIAN_POINT('Ctrl Pts',(-26.731907224948,24.0633754189928,-55.2179616053503));
#15417=CARTESIAN_POINT('Ctrl Pts',(-26.7295828783929,24.0775029746968,-55.2188374467544));
#15418=CARTESIAN_POINT('Ctrl Pts',(-26.7289073175066,24.0815605736646,-55.2190893252596));
#15419=CARTESIAN_POINT('Ctrl Pts',(-26.7276551751058,24.08899340521,-55.2195513268156));
#15420=CARTESIAN_POINT('Ctrl Pts',(-26.7270809784511,24.0923690384476,-55.2197613736964));
#15421=CARTESIAN_POINT('Ctrl Pts',(-26.725907954037,24.0991992447175,-55.2201868437949));
#15422=CARTESIAN_POINT('Ctrl Pts',(-26.725308866597,24.1026537674217,-55.2204022749987));
#15423=CARTESIAN_POINT('Ctrl Pts',(-26.7238229310854,24.1111398517284,-55.2209320795149));
#15424=CARTESIAN_POINT('Ctrl Pts',(-26.722929755159,24.1161702826921,-55.2212466542327));
#15425=CARTESIAN_POINT('Ctrl Pts',(-26.7196451928627,24.1344169868981,-55.2223895806019));
#15426=CARTESIAN_POINT('Ctrl Pts',(-26.7171831812246,24.1476202607189,-55.2232201832828));
#15427=CARTESIAN_POINT('Ctrl Pts',(-26.680120228734,24.3397102156873,-55.2353575426157));
#15428=CARTESIAN_POINT('Ctrl Pts',(-26.6304990414954,24.5153307830893,-55.2471564643207));
#15429=CARTESIAN_POINT('Ctrl Pts',(-26.4957117914711,24.8733336040978,-55.2726524478074));
#15430=CARTESIAN_POINT('Ctrl Pts',(-26.4077711531711,25.0538665935108,-55.2863697394559));
#15431=CARTESIAN_POINT('Ctrl Pts',(-26.2773788723654,25.2682318598123,-55.3031468688061));
#15432=CARTESIAN_POINT('Ctrl Pts',(-26.2501053471981,25.310782636509,-55.306501069829));
#15433=CARTESIAN_POINT('Ctrl Pts',(-26.2069997537772,25.3746746237673,-55.3115561877946));
#15434=CARTESIAN_POINT('Ctrl Pts',(-26.1918865368085,25.3964896886562,-55.3132855881141));
#15435=CARTESIAN_POINT('Ctrl Pts',(-26.1499063449645,25.4555146533904,-55.3179690113146));
#15436=CARTESIAN_POINT('Ctrl Pts',(-26.122509975173,25.4923431294445,-55.3208958796263));
#15437=CARTESIAN_POINT('Ctrl Pts',(-26.0912753038264,25.532510252206,-55.3240819153644));
#15438=CARTESIAN_POINT('Ctrl Pts',(-26.0882068998961,25.5364373228806,-55.3243933414484));
#15439=CARTESIAN_POINT('Ctrl Pts',(-26.0836080880757,25.5422950153119,-55.3248577496779));
#15440=CARTESIAN_POINT('Ctrl Pts',(-26.082084574046,25.5442310022417,-55.3250112183647));
#15441=CARTESIAN_POINT('Ctrl Pts',(-26.0794588151184,25.5475597922796,-55.3252750598111));
#15442=CARTESIAN_POINT('Ctrl Pts',(-26.078357638958,25.5489534307687,-55.3253855090895));
#15443=CARTESIAN_POINT('Ctrl Pts',(-26.076077356691,25.5518344357035,-55.3256138114504));
#15444=CARTESIAN_POINT('Ctrl Pts',(-26.074898090815,25.5533216682578,-55.3257316520467));
#15445=CARTESIAN_POINT('Ctrl Pts',(-26.0721208592695,25.5568178284469,-55.3260086394904));
#15446=CARTESIAN_POINT('Ctrl Pts',(-26.0705218016787,25.5588258957119,-55.3261677076128));
#15447=CARTESIAN_POINT('Ctrl Pts',(-26.0652978370602,25.5653699947338,-55.3266860269692));
#15448=CARTESIAN_POINT('Ctrl Pts',(-26.0616630432463,25.5698981742764,-55.3270445698347));
#15449=CARTESIAN_POINT('Ctrl Pts',(-25.9723215332929,25.6805845479778,-55.3358068096169));
#15450=CARTESIAN_POINT('Ctrl Pts',(-25.8799586128539,25.7812193526092,-55.3437312782584));
#15451=CARTESIAN_POINT('Ctrl Pts',(-25.5217700317589,26.1248943015793,-55.3719311850345));
#15452=CARTESIAN_POINT('Ctrl Pts',(-25.2221814632887,26.3287992394889,-55.3913060963372));
#15453=CARTESIAN_POINT('Ctrl Pts',(-24.8765276641856,26.487518074339,-55.4143074282496));
#15454=CARTESIAN_POINT('Ctrl Pts',(-24.8578890603224,26.4958630412873,-55.4155483190382));
#15455=CARTESIAN_POINT('Ctrl Pts',(-24.8334374239143,26.5065328384396,-55.4171774224722));
#15456=CARTESIAN_POINT('Ctrl Pts',(-24.827694869945,26.5090187933722,-55.4175601088675));
#15457=CARTESIAN_POINT('Ctrl Pts',(-24.8188369662787,26.5128227903177,-55.4181505482601));
#15458=CARTESIAN_POINT('Ctrl Pts',(-24.8157266984097,26.5141526882763,-55.4183578961229));
#15459=CARTESIAN_POINT('Ctrl Pts',(-24.8096394145586,26.5167441794213,-55.4187637645624));
#15460=CARTESIAN_POINT('Ctrl Pts',(-24.8066625816164,26.5180061944998,-55.4189622704626));
#15461=CARTESIAN_POINT('Ctrl Pts',(-24.8000728106564,26.5207882067102,-55.4194017602233));
#15462=CARTESIAN_POINT('Ctrl Pts',(-24.7964589925964,26.5223060949462,-55.4196428155479));
#15463=CARTESIAN_POINT('Ctrl Pts',(-24.7889704208909,26.5254354107681,-55.4201424180721));
#15464=CARTESIAN_POINT('Ctrl Pts',(-24.7850952729389,26.5270458696803,-55.4204009976828));
#15465=CARTESIAN_POINT('Ctrl Pts',(-24.7752003043774,26.5311354379836,-55.421061393388));
#15466=CARTESIAN_POINT('Ctrl Pts',(-24.7691761181068,26.5336038747811,-55.4214635711034));
#15467=CARTESIAN_POINT('Ctrl Pts',(-24.7518354393625,26.5406480036397,-55.4226216104398));
#15468=CARTESIAN_POINT('Ctrl Pts',(-24.7405004683905,26.5451776401428,-55.4233790271196));
#15469=CARTESIAN_POINT('Ctrl Pts',(-24.6307236361333,26.5883245938208,-55.4307192045059));
#15470=CARTESIAN_POINT('Ctrl Pts',(-24.5304734175282,26.6221350960552,-55.4374625312866));
#15471=CARTESIAN_POINT('Ctrl Pts',(-24.2823213188424,26.6924421937905,-55.4542668023194));
#15472=CARTESIAN_POINT('Ctrl Pts',(-24.1331501821021,26.7235004702846,-55.4644693184428));
#15473=CARTESIAN_POINT('Ctrl Pts',(-23.7535422485739,26.7748619488649,-55.4903708273433));
#15474=CARTESIAN_POINT('Ctrl Pts',(-23.5220394199463,26.7811438036041,-55.5061351802148));
#15475=CARTESIAN_POINT('Ctrl Pts',(-23.2785771804949,26.7615586497784,-55.521553168706));
#15476=CARTESIAN_POINT('Ctrl Pts',(-23.2653254117304,26.7604100093648,-55.5223885553856));
#15477=CARTESIAN_POINT('Ctrl Pts',(-23.2484387764477,26.7588409127376,-55.5234478805438));
#15478=CARTESIAN_POINT('Ctrl Pts',(-23.2447972471421,26.7584962897772,-55.5236760106748));
#15479=CARTESIAN_POINT('Ctrl Pts',(-23.2390142378174,26.7579390684238,-55.5240377987019));
#15480=CARTESIAN_POINT('Ctrl Pts',(-23.2368723843756,26.7577305248881,-55.5241716854019));
#15481=CARTESIAN_POINT('Ctrl Pts',(-23.2328732516013,26.7573371016268,-55.5244214650139));
#15482=CARTESIAN_POINT('Ctrl Pts',(-23.2310159363426,26.757152755017,-55.5245373871528));
#15483=CARTESIAN_POINT('Ctrl Pts',(-23.2268515496233,26.7567357678768,-55.5247971173852));
#15484=CARTESIAN_POINT('Ctrl Pts',(-23.2245445735581,26.7565022514155,-55.5249408749225));
#15485=CARTESIAN_POINT('Ctrl Pts',(-23.2177326041151,26.7558053030435,-55.5253649876561));
#15486=CARTESIAN_POINT('Ctrl Pts',(-23.2132283093705,26.7553348623535,-55.5256449464931));
#15487=CARTESIAN_POINT('Ctrl Pts',(-23.1782818843785,26.7516104793563,-55.5278133898286));
#15488=CARTESIAN_POINT('Ctrl Pts',(-23.1478852001811,26.747932248123,-55.5296782664915));
#15489=CARTESIAN_POINT('Ctrl Pts',(-23.0430531268668,26.7337281666625,-55.536050570907));
#15490=CARTESIAN_POINT('Ctrl Pts',(-22.9689319669206,26.721031068864,-55.5404526587042));
#15491=CARTESIAN_POINT('Ctrl Pts',(-22.6095691825573,26.646444034771,-55.5615807370014));
#15492=CARTESIAN_POINT('Ctrl Pts',(-22.3336753044659,26.5486994933522,-55.5772652750174));
#15493=CARTESIAN_POINT('Ctrl Pts',(-22.0750357439016,26.4155366348007,-55.5940940905011));
#15494=CARTESIAN_POINT('',(-26.7730018345793,23.5523722612815,-55.4357734493122));
#15495=CARTESIAN_POINT('Ctrl Pts',(-22.0750360153461,26.4155367745563,-55.8427674868566));
#15496=CARTESIAN_POINT('Ctrl Pts',(-22.1638033690836,26.4612394187782,-55.8366160816763));
#15497=CARTESIAN_POINT('Ctrl Pts',(-22.2547513529059,26.5028413659955,-55.830464676496));
#15498=CARTESIAN_POINT('Ctrl Pts',(-22.3474633730655,26.5401381151882,-55.8243132713157));
#15499=CARTESIAN_POINT('Ctrl Pts',(-22.4401518048246,26.5774253750973,-55.8181634312162));
#15500=CARTESIAN_POINT('Ctrl Pts',(-22.5346029781623,26.6104094517274,-55.8120135911168));
#15501=CARTESIAN_POINT('Ctrl Pts',(-22.6303797647384,26.6389337478629,-55.8058637510173));
#15502=CARTESIAN_POINT('Ctrl Pts',(-22.7261578061745,26.6674584177214,-55.7997138303432));
#15503=CARTESIAN_POINT('Ctrl Pts',(-22.8232610787732,26.6915230675885,-55.793563909669));
#15504=CARTESIAN_POINT('Ctrl Pts',(-22.9212376924382,26.7110210924237,-55.7874139889948));
#15505=CARTESIAN_POINT('Ctrl Pts',(-23.0192418011187,26.7305245889574,-55.7812623424786));
#15506=CARTESIAN_POINT('Ctrl Pts',(-23.1181193118339,26.7454588295939,-55.7751106959623));
#15507=CARTESIAN_POINT('Ctrl Pts',(-23.217409555345,26.7557685768256,-55.7689590494461));
#15508=CARTESIAN_POINT('Ctrl Pts',(-23.3168125741409,26.7660900340164,-55.7628004158013));
#15509=CARTESIAN_POINT('Ctrl Pts',(-23.416628828747,26.7717764704703,-55.7566417821566));
#15510=CARTESIAN_POINT('Ctrl Pts',(-23.51639415779,26.7728246678948,-55.7504831485119));
#15511=CARTESIAN_POINT('Ctrl Pts',(-23.6162263079814,26.7738735673844,-55.7443203899173));
#15512=CARTESIAN_POINT('Ctrl Pts',(-23.7160070313591,26.7702780593493,-55.7381576313228));
#15513=CARTESIAN_POINT('Ctrl Pts',(-23.8152758372828,26.7620869312227,-55.7319948727283));
#15514=CARTESIAN_POINT('Ctrl Pts',(-23.9146972370149,26.7538832118756,-55.7258226408778));
#15515=CARTESIAN_POINT('Ctrl Pts',(-24.0136047194735,26.7410698307426,-55.7196504090274));
#15516=CARTESIAN_POINT('Ctrl Pts',(-24.1115467365093,26.7237468799074,-55.7134781771769));
#15517=CARTESIAN_POINT('Ctrl Pts',(-24.1406837651828,26.7185934296266,-55.7116419836632));
#15518=CARTESIAN_POINT('Ctrl Pts',(-24.1697354460884,26.7130412109727,-55.7098057901494));
#15519=CARTESIAN_POINT('Ctrl Pts',(-24.1986901638857,26.7070937059787,-55.7079695966356));
#15520=CARTESIAN_POINT('Ctrl Pts',(-24.2960171399522,26.6871020527961,-55.7017975053233));
#15521=CARTESIAN_POINT('Ctrl Pts',(-24.3925901342158,26.6625700144652,-55.695625414011));
#15522=CARTESIAN_POINT('Ctrl Pts',(-24.487953024853,26.6335681736014,-55.6894533226986));
#15523=CARTESIAN_POINT('Ctrl Pts',(-24.5831867082013,26.6046056273647,-55.6832895939598));
#15524=CARTESIAN_POINT('Ctrl Pts',(-24.6772131348009,26.5711854410995,-55.6771258652211));
#15525=CARTESIAN_POINT('Ctrl Pts',(-24.7695860322198,26.533429257434,-55.6709621364823));
#15526=CARTESIAN_POINT('Ctrl Pts',(-24.8618610692233,26.4957130729017,-55.6648049376356));
#15527=CARTESIAN_POINT('Ctrl Pts',(-24.9524856598126,26.4536701868769,-55.6586477387889));
#15528=CARTESIAN_POINT('Ctrl Pts',(-25.0410293012036,26.4074718417912,-55.6524905399422));
#15529=CARTESIAN_POINT('Ctrl Pts',(-25.1295082225622,26.3613072648941,-55.6463378416345));
#15530=CARTESIAN_POINT('Ctrl Pts',(-25.2159088348528,26.3109934681144,-55.6401851433268));
#15531=CARTESIAN_POINT('Ctrl Pts',(-25.299822068589,26.2567491598225,-55.6340324450191));
#15532=CARTESIAN_POINT('Ctrl Pts',(-25.3837034823076,26.2025254210495,-55.6278820798234));
#15533=CARTESIAN_POINT('Ctrl Pts',(-25.465099027226,26.1443743678503,-55.6217317146276));
#15534=CARTESIAN_POINT('Ctrl Pts',(-25.5436264153047,26.0825594093533,-55.6155813494319));
#15535=CARTESIAN_POINT('Ctrl Pts',(-25.6221450340732,26.0207513538561,-55.6094316710597));
#15536=CARTESIAN_POINT('Ctrl Pts',(-25.6977957914518,25.9552804752095,-55.6032819926875));
#15537=CARTESIAN_POINT('Ctrl Pts',(-25.7702282607602,25.886451436937,-55.5971323143153));
#15538=CARTESIAN_POINT('Ctrl Pts',(-25.8426720190566,25.8176116712906,-55.5909816774828));
#15539=CARTESIAN_POINT('Ctrl Pts',(-25.9118961780703,25.7454130057018,-55.5848310406503));
#15540=CARTESIAN_POINT('Ctrl Pts',(-25.9775867989288,25.6701973228642,-55.5786804038178));
#15541=CARTESIAN_POINT('Ctrl Pts',(-26.0433476949519,25.5949011750466,-55.572523187096));
#15542=CARTESIAN_POINT('Ctrl Pts',(-26.1055672179356,25.5165818926573,-55.5663659703742));
#15543=CARTESIAN_POINT('Ctrl Pts',(-26.1639715048073,25.4356147494361,-55.5602087536524));
#15544=CARTESIAN_POINT('Ctrl Pts',(-26.2224083751914,25.3546024349773,-55.5540481018446));
#15545=CARTESIAN_POINT('Ctrl Pts',(-26.2770255331043,25.2709396815692,-55.5478874500368));
#15546=CARTESIAN_POINT('Ctrl Pts',(-26.3275934335353,25.1850292985527,-55.541726798229));
#15547=CARTESIAN_POINT('Ctrl Pts',(-26.3782459520459,25.0989751569153,-55.53555583746));
#15548=CARTESIAN_POINT('Ctrl Pts',(-26.4248354756847,25.0106662573898,-55.5293848766909));
#15549=CARTESIAN_POINT('Ctrl Pts',(-26.4671791846668,24.9205285855162,-55.5232139159219));
#15550=CARTESIAN_POINT('Ctrl Pts',(-26.4995009327744,24.8517248081585,-55.5185035057015));
#15551=CARTESIAN_POINT('Ctrl Pts',(-26.5293497993277,24.7818559668027,-55.5137930954811));
#15552=CARTESIAN_POINT('Ctrl Pts',(-26.5566640073031,24.7111175547814,-55.5090826852607));
#15553=CARTESIAN_POINT('Ctrl Pts',(-26.5974036268661,24.6056099743735,-55.5020570259212));
#15554=CARTESIAN_POINT('Ctrl Pts',(-26.6326230710418,24.4978581799752,-55.4950313665816));
#15555=CARTESIAN_POINT('Ctrl Pts',(-26.6621013805474,24.388413795647,-55.4880057072421));
#15556=CARTESIAN_POINT('Ctrl Pts',(-26.6914692696457,24.279379370156,-55.4810063647497));
#15557=CARTESIAN_POINT('Ctrl Pts',(-26.715138833174,24.1686651889649,-55.4740070222573));
#15558=CARTESIAN_POINT('Ctrl Pts',(-26.7329381736759,24.056838819333,-55.4670076797649));
#15559=CARTESIAN_POINT('Ctrl Pts',(-26.7506182001143,23.9457620537979,-55.4600552558645));
#15560=CARTESIAN_POINT('Ctrl Pts',(-26.7625063383809,23.8335881540695,-55.4531028319641));
#15561=CARTESIAN_POINT('Ctrl Pts',(-26.7684817941327,23.7208924358339,-55.4461504080637));
#15562=CARTESIAN_POINT('Ctrl Pts',(-26.7714547168977,23.664823797694,-55.4426914218132));
#15563=CARTESIAN_POINT('Ctrl Pts',(-26.7729648340919,23.6086262739736,-55.4392324355627));
#15564=CARTESIAN_POINT('Ctrl Pts',(-26.7730018345793,23.5523722612815,-55.4357734493122));
#15565=CARTESIAN_POINT('Ctrl Pts',(-26.7730019166452,23.5522435862346,-55.438005776981));
#15566=CARTESIAN_POINT('Ctrl Pts',(-26.7730788414302,23.4277320278056,-55.4308287226616));
#15567=CARTESIAN_POINT('Ctrl Pts',(-26.7659400990873,23.3033318469675,-55.4234862517857));
#15568=CARTESIAN_POINT('Ctrl Pts',(-26.7508314924961,23.1728145698253,-55.4154867208764));
#15569=CARTESIAN_POINT('Ctrl Pts',(-26.7500166883877,23.1659682101737,-55.4150662542082));
#15570=CARTESIAN_POINT('Ctrl Pts',(-26.7486509437576,23.1547981629762,-55.4143788482534));
#15571=CARTESIAN_POINT('Ctrl Pts',(-26.7481131876054,23.1504728609894,-55.4141123253738));
#15572=CARTESIAN_POINT('Ctrl Pts',(-26.7471500005202,23.142852018815,-55.4136421228204));
#15573=CARTESIAN_POINT('Ctrl Pts',(-26.7467282432011,23.1395560139398,-55.413438559509));
#15574=CARTESIAN_POINT('Ctrl Pts',(-26.745891205554,23.1330940191292,-55.4130390655293));
#15575=CARTESIAN_POINT('Ctrl Pts',(-26.7454763158846,23.1299279817351,-55.4128431474389));
#15576=CARTESIAN_POINT('Ctrl Pts',(-26.744642350688,23.123636556246,-55.4124534527456));
#15577=CARTESIAN_POINT('Ctrl Pts',(-26.7442233919184,23.1205111558416,-55.4122596800337));
#15578=CARTESIAN_POINT('Ctrl Pts',(-26.7432253087054,23.1131476186655,-55.4118027108634));
#15579=CARTESIAN_POINT('Ctrl Pts',(-26.74264233314,23.1089100172242,-55.4115393925674));
#15580=CARTESIAN_POINT('Ctrl Pts',(-26.7408948269966,23.0963921736642,-55.4107605415615));
#15581=CARTESIAN_POINT('Ctrl Pts',(-26.7397065119313,23.0881153366979,-55.410244255322));
#15582=CARTESIAN_POINT('Ctrl Pts',(-26.7289578143729,23.0152652444207,-55.4056884032595));
#15583=CARTESIAN_POINT('Ctrl Pts',(-26.717470397897,22.9509957819651,-55.401587917036));
#15584=CARTESIAN_POINT('Ctrl Pts',(-26.6997575563654,22.8667550128291,-55.3960997077482));
#15585=CARTESIAN_POINT('Ctrl Pts',(-26.695277759821,22.8464293710084,-55.3947667477626));
#15586=CARTESIAN_POINT('Ctrl Pts',(-26.6849237527349,22.8015253070283,-55.391802443156));
#15587=CARTESIAN_POINT('Ctrl Pts',(-26.6789567359544,22.7769698737841,-55.3901684302526));
#15588=CARTESIAN_POINT('Ctrl Pts',(-26.6680249324779,22.7341828297895,-55.3872985689068));
#15589=CARTESIAN_POINT('Ctrl Pts',(-26.6631873696385,22.7159197595268,-55.3860663444757));
#15590=CARTESIAN_POINT('Ctrl Pts',(-26.5856074258991,22.4331058238264,-55.3668729393034));
#15591=CARTESIAN_POINT('Ctrl Pts',(-26.4795321946045,22.1788719186732,-55.3479602111803));
#15592=CARTESIAN_POINT('Ctrl Pts',(-26.2942602041791,21.8573546179912,-55.3232728031932));
#15593=CARTESIAN_POINT('Ctrl Pts',(-26.2421890534913,21.7757206945836,-55.3169438300984));
#15594=CARTESIAN_POINT('Ctrl Pts',(-26.1814052385875,21.689276448931,-55.3102736863033));
#15595=CARTESIAN_POINT('Ctrl Pts',(-26.1762631643443,21.6820275160331,-55.3097146123015));
#15596=CARTESIAN_POINT('Ctrl Pts',(-26.1673443991041,21.6695640483446,-55.3087539526943));
#15597=CARTESIAN_POINT('Ctrl Pts',(-26.1635819791007,21.6643394332487,-55.3083514283213));
#15598=CARTESIAN_POINT('Ctrl Pts',(-26.1582326197687,21.6569578920223,-55.307783020954));
#15599=CARTESIAN_POINT('Ctrl Pts',(-26.1566586420436,21.6547916588555,-55.3076162486798));
#15600=CARTESIAN_POINT('Ctrl Pts',(-26.1539526610715,21.6510772166947,-55.3073303497236));
#15601=CARTESIAN_POINT('Ctrl Pts',(-26.1528219740959,21.6495280544568,-55.307211131046));
#15602=CARTESIAN_POINT('Ctrl Pts',(-26.1506569128562,21.6465672426875,-55.3069833152429));
#15603=CARTESIAN_POINT('Ctrl Pts',(-26.1496227730291,21.6451554282253,-55.3068747018983));
#15604=CARTESIAN_POINT('Ctrl Pts',(-26.1471899790904,21.6418398306759,-55.3066196650804));
#15605=CARTESIAN_POINT('Ctrl Pts',(-26.1457903783541,21.6399367384976,-55.3064733080106));
#15606=CARTESIAN_POINT('Ctrl Pts',(-26.1416681916828,21.6343445324399,-55.3060433209981));
#15607=CARTESIAN_POINT('Ctrl Pts',(-26.1389398095142,21.6306596679055,-55.3057600939712));
#15608=CARTESIAN_POINT('Ctrl Pts',(-26.1157714543348,21.5995084660861,-55.3033665040913));
#15609=CARTESIAN_POINT('Ctrl Pts',(-26.09490186822,21.5723623083113,-55.3012856774986));
#15610=CARTESIAN_POINT('Ctrl Pts',(-25.8790297762686,21.3006404161083,-55.2804504389529));
#15611=CARTESIAN_POINT('Ctrl Pts',(-25.649810790791,21.0853229235165,-55.2637472765753));
#15612=CARTESIAN_POINT('Ctrl Pts',(-25.325451797575,20.8592325712338,-55.2412600523618));
#15613=CARTESIAN_POINT('Ctrl Pts',(-25.2560038534857,20.8146845938912,-55.2365120392474));
#15614=CARTESIAN_POINT('Ctrl Pts',(-25.1366330269504,20.744427393235,-55.2283898372857));
#15615=CARTESIAN_POINT('Ctrl Pts',(-25.0876083371197,20.7172692358729,-55.2250648372415));
#15616=CARTESIAN_POINT('Ctrl Pts',(-25.020036635349,20.6821071592685,-55.2204834114644));
#15617=CARTESIAN_POINT('Ctrl Pts',(-25.0020841894197,20.6729781272969,-55.2192663863316));
#15618=CARTESIAN_POINT('Ctrl Pts',(-24.9715769729359,20.6578230524914,-55.2171979544852));
#15619=CARTESIAN_POINT('Ctrl Pts',(-24.9590664202684,20.6517089530563,-55.2163496386054));
#15620=CARTESIAN_POINT('Ctrl Pts',(-24.9418555921775,20.6434355040831,-55.2151823570006));
#15621=CARTESIAN_POINT('Ctrl Pts',(-24.9371890303002,20.6412060455931,-55.2148658341642));
#15622=CARTESIAN_POINT('Ctrl Pts',(-24.9296874494974,20.6376443049841,-55.2143569707075));
#15623=CARTESIAN_POINT('Ctrl Pts',(-24.9268558061352,20.6363049001396,-55.2141648777375));
#15624=CARTESIAN_POINT('Ctrl Pts',(-24.9209575027179,20.6335254407412,-55.2137647241773));
#15625=CARTESIAN_POINT('Ctrl Pts',(-24.9178905169802,20.632086089945,-55.2135566394893));
#15626=CARTESIAN_POINT('Ctrl Pts',(-24.9108376711355,20.6287897171977,-55.2130780930953));
#15627=CARTESIAN_POINT('Ctrl Pts',(-24.9068502751516,20.6269360143984,-55.2128075169102));
#15628=CARTESIAN_POINT('Ctrl Pts',(-24.8942052560412,20.6210889071935,-55.2119493648231));
#15629=CARTESIAN_POINT('Ctrl Pts',(-24.8855337592681,20.6171257863025,-55.2113607444296));
#15630=CARTESIAN_POINT('Ctrl Pts',(-24.8527804738253,20.6023319494138,-55.2091368715181));
#15631=CARTESIAN_POINT('Ctrl Pts',(-24.8285839942945,20.5917590968131,-55.2074927910047));
#15632=CARTESIAN_POINT('Ctrl Pts',(-24.7971014803647,20.5784608727237,-55.20535157885));
#15633=CARTESIAN_POINT('Ctrl Pts',(-24.7899312013358,20.5754626635764,-55.2048637719002));
#15634=CARTESIAN_POINT('Ctrl Pts',(-24.7789259015754,20.5709075628481,-55.2041148405568));
#15635=CARTESIAN_POINT('Ctrl Pts',(-24.7750985743412,20.5693320589545,-55.2038543429142));
#15636=CARTESIAN_POINT('Ctrl Pts',(-24.7680463882286,20.5664449297232,-55.203374276119));
#15637=CARTESIAN_POINT('Ctrl Pts',(-24.7648224144842,20.5651311468491,-55.2031547794513));
#15638=CARTESIAN_POINT('Ctrl Pts',(-24.7595673307763,20.5629996007606,-55.2027969503533));
#15639=CARTESIAN_POINT('Ctrl Pts',(-24.7575374989892,20.5621786764564,-55.20265872316));
#15640=CARTESIAN_POINT('Ctrl Pts',(-24.743198041339,20.556396370184,-55.2016821518189));
#15641=CARTESIAN_POINT('Ctrl Pts',(-24.7308588531329,20.551509059811,-55.2008413634327));
#15642=CARTESIAN_POINT('Ctrl Pts',(-24.7147835250829,20.5452565343593,-55.199745390408));
#15643=CARTESIAN_POINT('Ctrl Pts',(-24.7110744237798,20.5438217719408,-55.1994924721166));
#15644=CARTESIAN_POINT('Ctrl Pts',(-24.7027207497376,20.5406081498196,-55.1989227523591));
#15645=CARTESIAN_POINT('Ctrl Pts',(-24.6980747031955,20.538833171804,-55.1986058266526));
#15646=CARTESIAN_POINT('Ctrl Pts',(-24.6791161845141,20.5316404972538,-55.1973123181178));
#15647=CARTESIAN_POINT('Ctrl Pts',(-24.6647694935682,20.5263140914803,-55.1963328369763));
#15648=CARTESIAN_POINT('Ctrl Pts',(-24.6273075325131,20.5127086333113,-55.193773561933));
#15649=CARTESIAN_POINT('Ctrl Pts',(-24.6041349315619,20.5045913150729,-55.1921888434871));
#15650=CARTESIAN_POINT('Ctrl Pts',(-24.4174790607513,20.4415913390572,-55.179411192005));
#15651=CARTESIAN_POINT('Ctrl Pts',(-24.2499410037847,20.399652636781,-55.1678420258864));
#15652=CARTESIAN_POINT('Ctrl Pts',(-24.0607885016073,20.3681392566168,-55.1548685802093));
#15653=CARTESIAN_POINT('Ctrl Pts',(-24.0416762435035,20.3651317167911,-55.1535589881339));
#15654=CARTESIAN_POINT('Ctrl Pts',(-23.9268993234158,20.3481278808895,-55.1457046768733));
#15655=CARTESIAN_POINT('Ctrl Pts',(-23.8306686681147,20.3382698197236,-55.1391606584033));
#15656=CARTESIAN_POINT('Ctrl Pts',(-23.6494306216396,20.3279117581735,-55.1270460491798));
#15657=CARTESIAN_POINT('Ctrl Pts',(-23.564557504351,20.3264172141409,-55.1214593357059));
#15658=CARTESIAN_POINT('Ctrl Pts',(-23.4467437362076,20.3289963633774,-55.1139078212282));
#15659=CARTESIAN_POINT('Ctrl Pts',(-23.4137810692429,20.3302244070553,-55.1118172578896));
#15660=CARTESIAN_POINT('Ctrl Pts',(-23.3762373694884,20.3322007075804,-55.1094659224595));
#15661=CARTESIAN_POINT('Ctrl Pts',(-23.3716337189843,20.3324529512764,-55.1091781098905));
#15662=CARTESIAN_POINT('Ctrl Pts',(-23.3646986244983,20.3328478686577,-55.1087453251952));
#15663=CARTESIAN_POINT('Ctrl Pts',(-23.3623667935396,20.3329831976648,-55.1085999411309));
#15664=CARTESIAN_POINT('Ctrl Pts',(-23.3583477335912,20.3332208302443,-55.1083495955966));
#15665=CARTESIAN_POINT('Ctrl Pts',(-23.3566604400101,20.3333219260148,-55.1082445657382));
#15666=CARTESIAN_POINT('Ctrl Pts',(-23.3531569874141,20.3335346050236,-55.1080266322967));
#15667=CARTESIAN_POINT('Ctrl Pts',(-23.3513408481613,20.3336463985887,-55.1079137410367));
#15668=CARTESIAN_POINT('Ctrl Pts',(-23.3463618634332,20.3339571159993,-55.1076044704728));
#15669=CARTESIAN_POINT('Ctrl Pts',(-23.3431992043127,20.3341591677743,-55.107408268326));
#15670=CARTESIAN_POINT('Ctrl Pts',(-23.3310706699407,20.3349519843805,-55.1066567793178));
#15671=CARTESIAN_POINT('Ctrl Pts',(-23.3221068720183,20.3355755867138,-55.1061033279163));
#15672=CARTESIAN_POINT('Ctrl Pts',(-23.3053437686649,20.3368122473116,-55.1050717762917));
#15673=CARTESIAN_POINT('Ctrl Pts',(-23.2975438939927,20.3374162285512,-55.1045931943316));
#15674=CARTESIAN_POINT('Ctrl Pts',(-23.0075361621405,20.3609355476323,-55.086848490599));
#15675=CARTESIAN_POINT('Ctrl Pts',(-22.7295198439185,20.4209168937968,-55.0715056784077));
#15676=CARTESIAN_POINT('Ctrl Pts',(-22.3450008906723,20.55873645097,-55.0485540163455));
#15677=CARTESIAN_POINT('Ctrl Pts',(-22.2296855437849,20.6078217223761,-55.0414392860695));
#15678=CARTESIAN_POINT('Ctrl Pts',(-22.0626634456669,20.6907162988059,-55.0305404699118));
#15679=CARTESIAN_POINT('Ctrl Pts',(-22.0085919303924,20.7195016364711,-55.0269150355831));
#15680=CARTESIAN_POINT('Ctrl Pts',(-21.9366758121197,20.7604584821626,-55.021942909467));
#15681=CARTESIAN_POINT('Ctrl Pts',(-21.9180833534373,20.7712950998397,-55.0206435580063));
#15682=CARTESIAN_POINT('Ctrl Pts',(-21.891112836644,20.7873788990309,-55.0187376671126));
#15683=CARTESIAN_POINT('Ctrl Pts',(-21.8826479233375,20.7924798607604,-55.0181364308397));
#15684=CARTESIAN_POINT('Ctrl Pts',(-21.867512123065,20.8016958718324,-55.0170558206725));
#15685=CARTESIAN_POINT('Ctrl Pts',(-21.8608325058726,20.8057964890609,-55.0165769776159));
#15686=CARTESIAN_POINT('Ctrl Pts',(-21.8506952527969,20.8120707813777,-55.0158472585343));
#15687=CARTESIAN_POINT('Ctrl Pts',(-21.8472266470128,20.8142267500391,-55.0155970366446));
#15688=CARTESIAN_POINT('Ctrl Pts',(-21.8409635569935,20.818136200474,-55.0151442453898));
#15689=CARTESIAN_POINT('Ctrl Pts',(-21.8381676449661,20.8198873936839,-55.0149417609927));
#15690=CARTESIAN_POINT('Ctrl Pts',(-21.8321688661262,20.8236575095015,-55.0145065577025));
#15691=CARTESIAN_POINT('Ctrl Pts',(-21.8289668608311,20.8256777876243,-55.0142737886808));
#15692=CARTESIAN_POINT('Ctrl Pts',(-21.8203784771757,20.8311177381768,-55.0136481959883));
#15693=CARTESIAN_POINT('Ctrl Pts',(-21.8149987020533,20.8345477584185,-55.0132549874915));
#15694=CARTESIAN_POINT('Ctrl Pts',(-21.7915675492942,20.8495849707157,-55.0115365259029));
#15695=CARTESIAN_POINT('Ctrl Pts',(-21.7736225171508,20.8613561227983,-55.0102051526829));
#15696=CARTESIAN_POINT('Ctrl Pts',(-21.744969228358,20.8805634727127,-55.0080542241215));
#15697=CARTESIAN_POINT('Ctrl Pts',(-21.7341859906707,20.8878870820493,-55.0072389579501));
#15698=CARTESIAN_POINT('Ctrl Pts',(-21.7185770004402,20.8986271311568,-55.0060503200258));
#15699=CARTESIAN_POINT('Ctrl Pts',(-21.7137156524232,20.9019918181511,-55.0056789133326));
#15700=CARTESIAN_POINT('Ctrl Pts',(-21.7030002596851,20.9094519620394,-55.0048575714395));
#15701=CARTESIAN_POINT('Ctrl Pts',(-21.6971505316691,20.9135535383859,-55.0044074060597));
#15702=CARTESIAN_POINT('Ctrl Pts',(-21.6856533002675,20.9216720595383,-55.0035191129067));
#15703=CARTESIAN_POINT('Ctrl Pts',(-21.6800050176504,20.9256878387504,-55.0030810307344));
#15704=CARTESIAN_POINT('Ctrl Pts',(-21.6611914792114,20.9391553366922,-55.0016161886175));
#15705=CARTESIAN_POINT('Ctrl Pts',(-21.64808473415,20.9486880261494,-55.0005863898564));
#15706=CARTESIAN_POINT('Ctrl Pts',(-21.6216822609435,20.9681970400879,-54.9984929476786));
#15707=CARTESIAN_POINT('Ctrl Pts',(-21.6083907074072,20.9781781761958,-54.9974291452662));
#15708=CARTESIAN_POINT('Ctrl Pts',(-21.3723110804667,21.1583323876443,-54.9783558075725));
#15709=CARTESIAN_POINT('Ctrl Pts',(-21.1726161808175,21.356738432022,-54.9592074660605));
#15710=CARTESIAN_POINT('Ctrl Pts',(-20.978265687732,21.6079859767994,-54.9378351084374));
#15711=CARTESIAN_POINT('Ctrl Pts',(-20.9559035422299,21.6379583238226,-54.9353285745684));
#15712=CARTESIAN_POINT('Ctrl Pts',(-20.8694592131209,21.758129256705,-54.9254651651377));
#15713=CARTESIAN_POINT('Ctrl Pts',(-20.8095104187599,21.8512241639307,-54.9182290018173));
#15714=CARTESIAN_POINT('Ctrl Pts',(-20.7514261501566,21.9525273542276,-54.9109121477205));
#15715=CARTESIAN_POINT('Ctrl Pts',(-20.7484035626668,21.9578338640952,-54.9105304383355));
#15716=CARTESIAN_POINT('Ctrl Pts',(-20.7441054943487,21.9654297546196,-54.9099863177446));
#15717=CARTESIAN_POINT('Ctrl Pts',(-20.7428177177453,21.9677121070976,-54.9098231166405));
#15718=CARTESIAN_POINT('Ctrl Pts',(-20.7405974376398,21.9716583935015,-54.9095414422922));
#15719=CARTESIAN_POINT('Ctrl Pts',(-20.73966362619,21.973321586785,-54.9094228839347));
#15720=CARTESIAN_POINT('Ctrl Pts',(-20.7378696967476,21.9765233748084,-54.909194949417));
#15721=CARTESIAN_POINT('Ctrl Pts',(-20.7370093661627,21.9780618431444,-54.9090855593253));
#15722=CARTESIAN_POINT('Ctrl Pts',(-20.7349748691037,21.9817070073866,-54.9088266895198));
#15723=CARTESIAN_POINT('Ctrl Pts',(-20.7338018024313,21.9838143206466,-54.9086772812481));
#15724=CARTESIAN_POINT('Ctrl Pts',(-20.7303118502431,21.9901003132188,-54.9082323363515));
#15725=CARTESIAN_POINT('Ctrl Pts',(-20.7280018776429,21.9942828539311,-54.9079372433761));
#15726=CARTESIAN_POINT('Ctrl Pts',(-20.7066955065813,22.0330646798854,-54.9052098029002));
#15727=CARTESIAN_POINT('Ctrl Pts',(-20.6883259044694,22.0680069855144,-54.9028168116254));
#15728=CARTESIAN_POINT('Ctrl Pts',(-20.5825806803053,22.2784527723303,-54.8887324896534));
#15729=CARTESIAN_POINT('Ctrl Pts',(-20.5107153530718,22.4613153426098,-54.8778204621623));
#15730=CARTESIAN_POINT('Ctrl Pts',(-20.4129187962472,22.7973099613299,-54.8582677154784));
#15731=CARTESIAN_POINT('Ctrl Pts',(-20.3805583395989,22.9479069034931,-54.8496707300012));
#15732=CARTESIAN_POINT('Ctrl Pts',(-20.3475600247115,23.1819031022879,-54.8360330787821));
#15733=CARTESIAN_POINT('Ctrl Pts',(-20.3391829023584,23.2639820096189,-54.8312000775601));
#15734=CARTESIAN_POINT('Ctrl Pts',(-20.3321951690406,23.3741702855651,-54.8245998753853));
#15735=CARTESIAN_POINT('Ctrl Pts',(-20.3307896423446,23.4020743386149,-54.8229189802117));
#15736=CARTESIAN_POINT('Ctrl Pts',(-20.3292992981187,23.4419850335803,-54.8204999105333));
#15737=CARTESIAN_POINT('Ctrl Pts',(-20.3289184681319,23.4539798517247,-54.8197709581643));
#15738=CARTESIAN_POINT('Ctrl Pts',(-20.3283645248389,23.4751555991665,-54.8184805507042));
#15739=CARTESIAN_POINT('Ctrl Pts',(-20.328163636515,23.4843357143486,-54.8179199693434));
#15740=CARTESIAN_POINT('Ctrl Pts',(-20.3279252395536,23.4978751629369,-54.8170914302833));
#15741=CARTESIAN_POINT('Ctrl Pts',(-20.3278573380519,23.5022339714565,-54.8168244270591));
#15742=CARTESIAN_POINT('Ctrl Pts',(-20.327754862315,23.5097975551617,-54.816360641702));
#15743=CARTESIAN_POINT('Ctrl Pts',(-20.3277162242714,23.5130022766352,-54.8161639874212));
#15744=CARTESIAN_POINT('Ctrl Pts',(-20.3276488624914,23.5193783945405,-54.8157724302156));
#15745=CARTESIAN_POINT('Ctrl Pts',(-20.3276200396307,23.5225497866913,-54.8155775306142));
#15746=CARTESIAN_POINT('Ctrl Pts',(-20.3275628006328,23.5300692189667,-54.8151150749233));
#15747=CARTESIAN_POINT('Ctrl Pts',(-20.3275385026174,23.5344172765624,-54.8148473897773));
#15748=CARTESIAN_POINT('Ctrl Pts',(-20.3274840371801,23.5496975630152,-54.8139056999258));
#15749=CARTESIAN_POINT('Ctrl Pts',(-20.3275006974699,23.5606297901022,-54.8132302267463));
#15750=CARTESIAN_POINT('Ctrl Pts',(-20.3284576747963,23.705358280467,-54.8042642712462));
#15751=CARTESIAN_POINT('Ctrl Pts',(-20.3376734622503,23.8389516442154,-54.7957129714449));
#15752=CARTESIAN_POINT('Ctrl Pts',(-20.3718405376574,24.0980590909349,-54.7785697743708));
#15753=CARTESIAN_POINT('Ctrl Pts',(-20.3960147901411,24.2234348499318,-54.7700139510418));
#15754=CARTESIAN_POINT('Ctrl Pts',(-20.4660134089959,24.4977676994828,-54.7508803302058));
#15755=CARTESIAN_POINT('Ctrl Pts',(-20.5153371595481,24.6455186445221,-54.7402921100955));
#15756=CARTESIAN_POINT('Ctrl Pts',(-20.6001468968037,24.8491851104599,-54.7256985386063));
#15757=CARTESIAN_POINT('Ctrl Pts',(-20.6269677103267,24.908470551591,-54.7214525293368));
#15758=CARTESIAN_POINT('Ctrl Pts',(-20.6680102227588,24.9923337262186,-54.7154891998209));
#15759=CARTESIAN_POINT('Ctrl Pts',(-20.6807887905279,25.0175960062414,-54.7136986383152));
#15760=CARTESIAN_POINT('Ctrl Pts',(-20.6959557888364,25.0466239396076,-54.7116507374985));
#15761=CARTESIAN_POINT('Ctrl Pts',(-20.6980206272203,25.0505559844579,-54.7113735394475));
#15762=CARTESIAN_POINT('Ctrl Pts',(-20.7011674003905,25.0565183680227,-54.710953534378));
#15763=CARTESIAN_POINT('Ctrl Pts',(-20.7022433811847,25.0585518169158,-54.7108103509092));
#15764=CARTESIAN_POINT('Ctrl Pts',(-20.7041957375733,25.0622319517613,-54.7105513245167));
#15765=CARTESIAN_POINT('Ctrl Pts',(-20.7050713627572,25.0638790239467,-54.7104354343239));
#15766=CARTESIAN_POINT('Ctrl Pts',(-20.7068339756456,25.0671876077352,-54.7102027166283));
#15767=CARTESIAN_POINT('Ctrl Pts',(-20.7077209862553,25.0688490953128,-54.7100858913388));
#15768=CARTESIAN_POINT('Ctrl Pts',(-20.7102540255229,25.0735838159427,-54.7097530862078));
#15769=CARTESIAN_POINT('Ctrl Pts',(-20.7119035916056,25.0766551690073,-54.7095373325529));
#15770=CARTESIAN_POINT('Ctrl Pts',(-20.7189650859787,25.089752048371,-54.7086178559576));
#15771=CARTESIAN_POINT('Ctrl Pts',(-20.7244252588212,25.0997516750192,-54.7079171798722));
#15772=CARTESIAN_POINT('Ctrl Pts',(-20.8201882261588,25.2729397993269,-54.6958017608508));
#15773=CARTESIAN_POINT('Ctrl Pts',(-20.9244517948233,25.4280425295136,-54.685249744017));
#15774=CARTESIAN_POINT('Ctrl Pts',(-21.2331744594496,25.8108804368285,-54.6576948031303));
#15775=CARTESIAN_POINT('Ctrl Pts',(-21.4575347825304,26.0200296116876,-54.6408473440662));
#15776=CARTESIAN_POINT('Ctrl Pts',(-21.7178504478405,26.2013967572225,-54.6216316628998));
#15777=CARTESIAN_POINT('Ctrl Pts',(-21.7277873911295,26.2082374651995,-54.6208989126937));
#15778=CARTESIAN_POINT('Ctrl Pts',(-21.7430999128358,26.2186525473302,-54.6197708305971));
#15779=CARTESIAN_POINT('Ctrl Pts',(-21.7484482851394,26.2222668818498,-54.6193770106708));
#15780=CARTESIAN_POINT('Ctrl Pts',(-21.7584021042008,26.2289500203174,-54.6186444236135));
#15781=CARTESIAN_POINT('Ctrl Pts',(-21.7630046743468,26.2320230822573,-54.6183058185895));
#15782=CARTESIAN_POINT('Ctrl Pts',(-21.7705852196155,26.2370563078044,-54.6177483443471));
#15783=CARTESIAN_POINT('Ctrl Pts',(-21.7735585853912,26.2390234207827,-54.6175297372139));
#15784=CARTESIAN_POINT('Ctrl Pts',(-21.7793642908342,26.2428505118196,-54.6171029948586));
#15785=CARTESIAN_POINT('Ctrl Pts',(-21.7821963127549,26.2447109653543,-54.6168948778723));
#15786=CARTESIAN_POINT('Ctrl Pts',(-21.788712923064,26.2489772553388,-54.6164160983547));
#15787=CARTESIAN_POINT('Ctrl Pts',(-21.7923995093482,26.2513800144884,-54.6161453209771));
#15788=CARTESIAN_POINT('Ctrl Pts',(-21.8041036336893,26.258974152679,-54.6152859009329));
#15789=CARTESIAN_POINT('Ctrl Pts',(-21.8121392797049,26.2641374065741,-54.6146962093826));
#15790=CARTESIAN_POINT('Ctrl Pts',(-21.8808987598081,26.3078877316409,-54.6096531571899));
#15791=CARTESIAN_POINT('Ctrl Pts',(-21.9428718063461,26.344464364874,-54.6051258761946));
#15792=CARTESIAN_POINT('Ctrl Pts',(-22.0288733983659,26.3914145198979,-54.5988597519354));
#15793=CARTESIAN_POINT('Ctrl Pts',(-22.0518827698974,26.4036161247636,-54.5971849162755));
#15794=CARTESIAN_POINT('Ctrl Pts',(-22.0750360179885,26.4155367759168,-54.5955012513333));
#15795=CARTESIAN_POINT('Origin',(-23.5502525316942,23.5502525316942,-77.3107734492734));
#15796=CARTESIAN_POINT('',(-22.0750356956303,26.4155366099478,-53.096872577003));
#15797=CARTESIAN_POINT('',(-22.0750361378578,26.4155368376325,-53.3407994113682));
#15798=CARTESIAN_POINT('',(-22.0750360153461,26.4155367745563,-77.3107734492734));
#15799=CARTESIAN_POINT('',(-26.7730023566686,23.5491903981972,-53.9421167188325));
#15800=CARTESIAN_POINT('Ctrl Pts',(-22.0750356956303,26.4155366099478,-53.096872577003));
#15801=CARTESIAN_POINT('Ctrl Pts',(-21.9264125543873,26.3390166718885,-53.1081849636288));
#15802=CARTESIAN_POINT('Ctrl Pts',(-21.7838852981894,26.2510064584347,-53.1194618737691));
#15803=CARTESIAN_POINT('Ctrl Pts',(-21.644761491229,26.1493381498409,-53.1304977873125));
#15804=CARTESIAN_POINT('Ctrl Pts',(-21.6407642551953,26.1464028891144,-53.130814879377));
#15805=CARTESIAN_POINT('Ctrl Pts',(-21.6326837681245,26.1404404468286,-53.1314558885018));
#15806=CARTESIAN_POINT('Ctrl Pts',(-21.6286008681162,26.1374128056937,-53.1317797777548));
#15807=CARTESIAN_POINT('Ctrl Pts',(-21.6180178841249,26.1295262063868,-53.1326192730615));
#15808=CARTESIAN_POINT('Ctrl Pts',(-21.6115289125131,26.1246522974172,-53.1331339772478));
#15809=CARTESIAN_POINT('Ctrl Pts',(-21.6016557715084,26.117178015854,-53.1339169743418));
#15810=CARTESIAN_POINT('Ctrl Pts',(-21.5982582964917,26.1145953873281,-53.1341863884835));
#15811=CARTESIAN_POINT('Ctrl Pts',(-21.585629747171,26.1049560148004,-53.1351876861482));
#15812=CARTESIAN_POINT('Ctrl Pts',(-21.5764315805592,26.0978560005917,-53.1359167442937));
#15813=CARTESIAN_POINT('Ctrl Pts',(-21.5645024581978,26.0885445855169,-53.1368617121533));
#15814=CARTESIAN_POINT('Ctrl Pts',(-21.5617365877379,26.0863783656786,-53.1370807724197));
#15815=CARTESIAN_POINT('Ctrl Pts',(-21.557489151381,26.08304056864,-53.1374171075578));
#15816=CARTESIAN_POINT('Ctrl Pts',(-21.5560050751758,26.0818722132867,-53.1375346121952));
#15817=CARTESIAN_POINT('Ctrl Pts',(-21.5530867203241,26.0795705476653,-53.1377656523878));
#15818=CARTESIAN_POINT('Ctrl Pts',(-21.5516523866666,26.0784373280153,-53.1378791929288));
#15819=CARTESIAN_POINT('Ctrl Pts',(-21.5484721537288,26.0759203332508,-53.1381309095772));
#15820=CARTESIAN_POINT('Ctrl Pts',(-21.5467267289484,26.0745359712531,-53.138269042315));
#15821=CARTESIAN_POINT('Ctrl Pts',(-21.5431004575973,26.0716537086574,-53.1385559902889));
#15822=CARTESIAN_POINT('Ctrl Pts',(-21.5412198480975,26.0701555099996,-53.1387047840066));
#15823=CARTESIAN_POINT('Ctrl Pts',(-21.5363783500534,26.0662896370802,-53.1390877979437));
#15824=CARTESIAN_POINT('Ctrl Pts',(-21.5334199490057,26.0639188319239,-53.1393217953335));
#15825=CARTESIAN_POINT('Ctrl Pts',(-21.5248120560862,26.0569956542946,-53.1400025401155));
#15826=CARTESIAN_POINT('Ctrl Pts',(-21.519173700073,26.0524293809648,-53.1404483114529));
#15827=CARTESIAN_POINT('Ctrl Pts',(-21.4609426211798,26.0049438970312,-53.1450512980499));
#15828=CARTESIAN_POINT('Ctrl Pts',(-21.409698582786,25.96038861478,-53.1490953338779));
#15829=CARTESIAN_POINT('Ctrl Pts',(-21.3276489647413,25.8843655462217,-53.1556329165519));
#15830=CARTESIAN_POINT('Ctrl Pts',(-21.2960152860911,25.8538290771929,-53.1581697852802));
#15831=CARTESIAN_POINT('Ctrl Pts',(-21.0608773142502,25.6173628954903,-53.1772424018582));
#15832=CARTESIAN_POINT('Ctrl Pts',(-20.8853333523026,25.3855054672074,-53.1928690626812));
#15833=CARTESIAN_POINT('Ctrl Pts',(-20.6933165665967,25.0450134271123,-53.2155987286319));
#15834=CARTESIAN_POINT('Ctrl Pts',(-20.6477209559888,24.9544250441392,-53.221612652192));
#15835=CARTESIAN_POINT('Ctrl Pts',(-20.6026431666172,24.8532510427292,-53.2283541414504));
#15836=CARTESIAN_POINT('Ctrl Pts',(-20.5988516485134,24.8446399978957,-53.2289280862801));
#15837=CARTESIAN_POINT('Ctrl Pts',(-20.5932865901723,24.831849424511,-53.2297808990881));
#15838=CARTESIAN_POINT('Ctrl Pts',(-20.5914840625612,24.827682498745,-53.2300587752421));
#15839=CARTESIAN_POINT('Ctrl Pts',(-20.588417214673,24.8205515128383,-53.2305343969663));
#15840=CARTESIAN_POINT('Ctrl Pts',(-20.5871485201455,24.8175893311604,-53.2307319929255));
#15841=CARTESIAN_POINT('Ctrl Pts',(-20.5846920216929,24.8118299803954,-53.2311162275239));
#15842=CARTESIAN_POINT('Ctrl Pts',(-20.583503727012,24.8090330238254,-53.2313028491362));
#15843=CARTESIAN_POINT('Ctrl Pts',(-20.5806758411265,24.8023506214307,-53.231748776472));
#15844=CARTESIAN_POINT('Ctrl Pts',(-20.5790399201579,24.7984636373417,-53.2320082068354));
#15845=CARTESIAN_POINT('Ctrl Pts',(-20.5741749926794,24.7868407071785,-53.2327841035234));
#15846=CARTESIAN_POINT('Ctrl Pts',(-20.5709685538065,24.7790954064949,-53.2333013358714));
#15847=CARTESIAN_POINT('Ctrl Pts',(-20.543896225,24.7129721410528,-53.2377188119685));
#15848=CARTESIAN_POINT('Ctrl Pts',(-20.5217199718412,24.6539213032495,-53.2416758496819));
#15849=CARTESIAN_POINT('Ctrl Pts',(-20.4700054336758,24.5028922651448,-53.2518372658197));
#15850=CARTESIAN_POINT('Ctrl Pts',(-20.4428450475918,24.4101713694486,-53.2581144346053));
#15851=CARTESIAN_POINT('Ctrl Pts',(-20.3387038807127,23.9846541524688,-53.287059718394));
#15852=CARTESIAN_POINT('Ctrl Pts',(-20.3107654224717,23.6421731156019,-53.3110069177333));
#15853=CARTESIAN_POINT('Ctrl Pts',(-20.3373648897722,23.2982956069008,-53.3328102903745));
#15854=CARTESIAN_POINT('Ctrl Pts',(-20.3376344562879,23.2948814421683,-53.333026512313));
#15855=CARTESIAN_POINT('Ctrl Pts',(-20.3388772123724,23.2794548856592,-53.3340023334152));
#15856=CARTESIAN_POINT('Ctrl Pts',(-20.3399123536812,23.2674473708176,-53.334758712591));
#15857=CARTESIAN_POINT('Ctrl Pts',(-20.3413408348653,23.2518970663943,-53.3357339068266));
#15858=CARTESIAN_POINT('Ctrl Pts',(-20.3416727088271,23.2483489339966,-53.3359561242431));
#15859=CARTESIAN_POINT('Ctrl Pts',(-20.3421904506979,23.242910941653,-53.3362962443138));
#15860=CARTESIAN_POINT('Ctrl Pts',(-20.3423721034959,23.2410206980787,-53.3364143850099));
#15861=CARTESIAN_POINT('Ctrl Pts',(-20.3427318043936,23.2373121470302,-53.3366460023423));
#15862=CARTESIAN_POINT('Ctrl Pts',(-20.3429097270817,23.2354938397536,-53.3367594851252));
#15863=CARTESIAN_POINT('Ctrl Pts',(-20.3433073192287,23.231465930234,-53.3370106962435));
#15864=CARTESIAN_POINT('Ctrl Pts',(-20.3435277255814,23.2292564087303,-53.3371483819689));
#15865=CARTESIAN_POINT('Ctrl Pts',(-20.3439897049508,23.2246731383995,-53.3374337480011));
#15866=CARTESIAN_POINT('Ctrl Pts',(-20.3442316310094,23.2222994253596,-53.3375814082492));
#15867=CARTESIAN_POINT('Ctrl Pts',(-20.3448602793852,23.2161984745238,-53.3379605894456));
#15868=CARTESIAN_POINT('Ctrl Pts',(-20.3452508680339,23.2124716255692,-53.3381918937985));
#15869=CARTESIAN_POINT('Ctrl Pts',(-20.3464045498224,23.2016458065126,-53.3388628724425));
#15870=CARTESIAN_POINT('Ctrl Pts',(-20.3471847408823,23.1945486246428,-53.3393016042207));
#15871=CARTESIAN_POINT('Ctrl Pts',(-20.3499204864417,23.1704013936626,-53.3407906016417));
#15872=CARTESIAN_POINT('Ctrl Pts',(-20.3519886820548,23.1533640535193,-53.3418348464376));
#15873=CARTESIAN_POINT('Ctrl Pts',(-20.3607321029306,23.0858504191379,-53.3459506001339));
#15874=CARTESIAN_POINT('Ctrl Pts',(-20.3684673368163,23.0355162121156,-53.3489696532923));
#15875=CARTESIAN_POINT('Ctrl Pts',(-20.3850972313087,22.9421063611589,-53.3545150781536));
#15876=CARTESIAN_POINT('Ctrl Pts',(-20.3936868526397,22.8989897321121,-53.3570517590737));
#15877=CARTESIAN_POINT('Ctrl Pts',(-20.4654737931617,22.5735458787382,-53.3761126821695));
#15878=CARTESIAN_POINT('Ctrl Pts',(-20.5655454780846,22.3007114592981,-53.3917287117786));
#15879=CARTESIAN_POINT('Ctrl Pts',(-20.7481484243374,21.9550561318075,-53.414457433548));
#15880=CARTESIAN_POINT('Ctrl Pts',(-20.799820491099,21.8675287569679,-53.4204843362831));
#15881=CARTESIAN_POINT('Ctrl Pts',(-20.8606991045604,21.7747220338233,-53.4272398258827));
#15882=CARTESIAN_POINT('Ctrl Pts',(-20.8658970600626,21.7668731875153,-53.4278140848418));
#15883=CARTESIAN_POINT('Ctrl Pts',(-20.8736533797484,21.7552719840823,-53.428667290215));
#15884=CARTESIAN_POINT('Ctrl Pts',(-20.8761854387927,21.7515020295901,-53.4289452435505));
#15885=CARTESIAN_POINT('Ctrl Pts',(-20.8805279841499,21.7450658961626,-53.4294209634691));
#15886=CARTESIAN_POINT('Ctrl Pts',(-20.8823345220245,21.7423970500725,-53.4296185803054));
#15887=CARTESIAN_POINT('Ctrl Pts',(-20.8858522327515,21.7372169987342,-53.4300028279046));
#15888=CARTESIAN_POINT('Ctrl Pts',(-20.8875629603889,21.7347054946978,-53.4301894415971));
#15889=CARTESIAN_POINT('Ctrl Pts',(-20.8916558028042,21.7287150566131,-53.4306353061616));
#15890=CARTESIAN_POINT('Ctrl Pts',(-20.8940411930921,21.725238377119,-53.4308946815753));
#15891=CARTESIAN_POINT('Ctrl Pts',(-20.9011870660204,21.7148670354655,-53.4316702551496));
#15892=CARTESIAN_POINT('Ctrl Pts',(-20.9059675926914,21.7079862858899,-53.4321872183806));
#15893=CARTESIAN_POINT('Ctrl Pts',(-20.9468778822758,21.6495902295827,-53.4365953915076));
#15894=CARTESIAN_POINT('Ctrl Pts',(-20.984480157522,21.5991277348869,-53.440543129246));
#15895=CARTESIAN_POINT('Ctrl Pts',(-21.0832386849365,21.4743883688339,-53.4506697109949));
#15896=CARTESIAN_POINT('Ctrl Pts',(-21.1462850435764,21.4016933108215,-53.4569205757691));
#15897=CARTESIAN_POINT('Ctrl Pts',(-21.241047465615,21.3018282673034,-53.4660153498107));
#15898=CARTESIAN_POINT('Ctrl Pts',(-21.2701903906715,21.2722805904828,-53.4687747355142));
#15899=CARTESIAN_POINT('Ctrl Pts',(-21.3267255778722,21.2171322341095,-53.4740534978926));
#15900=CARTESIAN_POINT('Ctrl Pts',(-21.3540102255009,21.1914303523533,-53.4765698617017));
#15901=CARTESIAN_POINT('Ctrl Pts',(-21.5759287172132,20.9895740786083,-53.4967728089937));
#15902=CARTESIAN_POINT('Ctrl Pts',(-21.7909848996853,20.8373159493884,-53.5148553221601));
#15903=CARTESIAN_POINT('Ctrl Pts',(-22.0252407489064,20.7111560143273,-53.5316767484546));
#15904=CARTESIAN_POINT('Ctrl Pts',(-22.0283450965297,20.7094907092915,-53.5318991745569));
#15905=CARTESIAN_POINT('Ctrl Pts',(-22.042112554287,20.7021343001088,-53.5328834179548));
#15906=CARTESIAN_POINT('Ctrl Pts',(-22.0528050866042,20.6964980200435,-53.5336420120053));
#15907=CARTESIAN_POINT('Ctrl Pts',(-22.066694584259,20.6892761062412,-53.5346196520834));
#15908=CARTESIAN_POINT('Ctrl Pts',(-22.0698626419416,20.6876355358304,-53.5348421212936));
#15909=CARTESIAN_POINT('Ctrl Pts',(-22.0747218628629,20.6851294249309,-53.5351825431785));
#15910=CARTESIAN_POINT('Ctrl Pts',(-22.076411064891,20.6842601202692,-53.5353007345611));
#15911=CARTESIAN_POINT('Ctrl Pts',(-22.0797264910376,20.6825576272401,-53.5355324174726));
#15912=CARTESIAN_POINT('Ctrl Pts',(-22.0813526467957,20.6817243325192,-53.5356459152116));
#15913=CARTESIAN_POINT('Ctrl Pts',(-22.084947275341,20.6798861870017,-53.5358964973556));
#15914=CARTESIAN_POINT('Ctrl Pts',(-22.0869160685292,20.6788819804275,-53.5360335403902));
#15915=CARTESIAN_POINT('Ctrl Pts',(-22.0910076325528,20.6768003302778,-53.5363179286341));
#15916=CARTESIAN_POINT('Ctrl Pts',(-22.0931305683855,20.6757232113315,-53.5364652532615));
#15917=CARTESIAN_POINT('Ctrl Pts',(-22.0985867036918,20.6729625166148,-53.5368432997671));
#15918=CARTESIAN_POINT('Ctrl Pts',(-22.1019216509747,20.6712823742681,-53.5370738068801));
#15919=CARTESIAN_POINT('Ctrl Pts',(-22.1116109496371,20.6664220144751,-53.5377418990032));
#15920=CARTESIAN_POINT('Ctrl Pts',(-22.117972957744,20.6632569865083,-53.5381785512955));
#15921=CARTESIAN_POINT('Ctrl Pts',(-22.1396363846814,20.6525689095394,-53.5396587330491));
#15922=CARTESIAN_POINT('Ctrl Pts',(-22.1549873235745,20.6451461109461,-53.540696321814));
#15923=CARTESIAN_POINT('Ctrl Pts',(-22.2172599425824,20.6156422599032,-53.5448628604659));
#15924=CARTESIAN_POINT('Ctrl Pts',(-22.2646550129647,20.5945721767084,-53.5479370047374));
#15925=CARTESIAN_POINT('Ctrl Pts',(-22.3783812312209,20.5472673143048,-53.5551329698665));
#15926=CARTESIAN_POINT('Ctrl Pts',(-22.445116130622,20.5220720286719,-53.5592135194819));
#15927=CARTESIAN_POINT('Ctrl Pts',(-22.8435373530829,20.3865789093105,-53.5830402699131));
#15928=CARTESIAN_POINT('Ctrl Pts',(-23.1905040045684,20.3286292295946,-53.6019433950894));
#15929=CARTESIAN_POINT('Ctrl Pts',(-23.5604852819765,20.3274537557524,-53.6243169797322));
#15930=CARTESIAN_POINT('Ctrl Pts',(-23.5809568112275,20.3275837810245,-53.6255609157499));
#15931=CARTESIAN_POINT('Ctrl Pts',(-23.6076881939732,20.3280082919943,-53.6271934627104));
#15932=CARTESIAN_POINT('Ctrl Pts',(-23.6139506973439,20.3281260074252,-53.6275765182799));
#15933=CARTESIAN_POINT('Ctrl Pts',(-23.6235958762808,20.3283354366992,-53.6281674022251));
#15934=CARTESIAN_POINT('Ctrl Pts',(-23.6269788414485,20.3284142231398,-53.6283748244781));
#15935=CARTESIAN_POINT('Ctrl Pts',(-23.6337034153293,20.3285814301208,-53.628787483053));
#15936=CARTESIAN_POINT('Ctrl Pts',(-23.6370450232457,20.3286697219609,-53.6289927150784));
#15937=CARTESIAN_POINT('Ctrl Pts',(-23.6444351372475,20.3288764897229,-53.6294469772071));
#15938=CARTESIAN_POINT('Ctrl Pts',(-23.6484835647494,20.328997398849,-53.6296960834212));
#15939=CARTESIAN_POINT('Ctrl Pts',(-23.6601128506016,20.3293666591382,-53.630412387059));
#15940=CARTESIAN_POINT('Ctrl Pts',(-23.667693036369,20.3296341407657,-53.6308801846923));
#15941=CARTESIAN_POINT('Ctrl Pts',(-23.7175271396097,20.3315688034118,-53.633961591426));
#15942=CARTESIAN_POINT('Ctrl Pts',(-23.7597440192034,20.3340406638312,-53.6366003744818));
#15943=CARTESIAN_POINT('Ctrl Pts',(-23.8841588440679,20.3437852520706,-53.6444653790937));
#15944=CARTESIAN_POINT('Ctrl Pts',(-23.9661348882302,20.3533844153971,-53.649762721159));
#15945=CARTESIAN_POINT('Ctrl Pts',(-24.141079906918,20.3807126067578,-53.6613164350819));
#15946=CARTESIAN_POINT('Ctrl Pts',(-24.2338189079287,20.3994121546459,-53.667594662097));
#15947=CARTESIAN_POINT('Ctrl Pts',(-24.3534955823353,20.4290757703748,-53.6758678729871));
#15948=CARTESIAN_POINT('Ctrl Pts',(-24.3813011251624,20.4363639704456,-53.6778021578916));
#15949=CARTESIAN_POINT('Ctrl Pts',(-24.4324512431185,20.4505050046481,-53.6813807688069));
#15950=CARTESIAN_POINT('Ctrl Pts',(-24.455823059852,20.45725215957,-53.6830238553027));
#15951=CARTESIAN_POINT('Ctrl Pts',(-24.499289462612,20.4703352762356,-53.6860930076009));
#15952=CARTESIAN_POINT('Ctrl Pts',(-24.5194027445228,20.4766049824001,-53.6875185943597));
#15953=CARTESIAN_POINT('Ctrl Pts',(-24.5938235606372,20.500606535501,-53.6928113428409));
#15954=CARTESIAN_POINT('Ctrl Pts',(-24.6477185820383,20.5195843617657,-53.6966802083909));
#15955=CARTESIAN_POINT('Ctrl Pts',(-24.7905314555467,20.5741818709959,-53.7069931870938));
#15956=CARTESIAN_POINT('Ctrl Pts',(-24.8784191951728,20.6123512343379,-53.713405570235));
#15957=CARTESIAN_POINT('Ctrl Pts',(-25.0244644449832,20.6836739313318,-53.7240403648126));
#15958=CARTESIAN_POINT('Ctrl Pts',(-25.0835283808606,20.7148265720418,-53.7283347501345));
#15959=CARTESIAN_POINT('Ctrl Pts',(-25.1467845617617,20.7507456523154,-53.7328926732911));
#15960=CARTESIAN_POINT('Ctrl Pts',(-25.1519741743764,20.7537116198804,-53.7332663001447));
#15961=CARTESIAN_POINT('Ctrl Pts',(-25.1592389363151,20.7578904332408,-53.7337888587177));
#15962=CARTESIAN_POINT('Ctrl Pts',(-25.161320985278,20.7590911646118,-53.7339385675561));
#15963=CARTESIAN_POINT('Ctrl Pts',(-25.1649257387841,20.7611754269837,-53.7341976692808));
#15964=CARTESIAN_POINT('Ctrl Pts',(-25.1664490623208,20.7620578763412,-53.7343071325014));
#15965=CARTESIAN_POINT('Ctrl Pts',(-25.1695893020679,20.7638804307699,-53.734532721381));
#15966=CARTESIAN_POINT('Ctrl Pts',(-25.1712061211877,20.7648206941833,-53.734648835973));
#15967=CARTESIAN_POINT('Ctrl Pts',(-25.1750239882963,20.767045430027,-53.7349229427272));
#15968=CARTESIAN_POINT('Ctrl Pts',(-25.1772243392184,20.7683311103401,-53.7350808559368));
#15969=CARTESIAN_POINT('Ctrl Pts',(-25.1818847800201,20.7710616587359,-53.7354151951705));
#15970=CARTESIAN_POINT('Ctrl Pts',(-25.1843444831164,20.7725071876143,-53.7355915781458));
#15971=CARTESIAN_POINT('Ctrl Pts',(-25.1909996745928,20.7764302382418,-53.7360686195069));
#15972=CARTESIAN_POINT('Ctrl Pts',(-25.195191490119,20.7789140236145,-53.7363688757136));
#15973=CARTESIAN_POINT('Ctrl Pts',(-25.2081620529372,20.7866392952875,-53.7372973419572));
#15974=CARTESIAN_POINT('Ctrl Pts',(-25.2169216045372,20.7919131201758,-53.7379235133485));
#15975=CARTESIAN_POINT('Ctrl Pts',(-25.2495369074405,20.8117617647422,-53.7402523541918));
#15976=CARTESIAN_POINT('Ctrl Pts',(-25.2732285651983,20.8266055692244,-53.7419387083908));
#15977=CARTESIAN_POINT('Ctrl Pts',(-25.3572506104525,20.8807840408662,-53.7479114250149));
#15978=CARTESIAN_POINT('Ctrl Pts',(-25.4164554231788,20.9218324164873,-53.7521053832842));
#15979=CARTESIAN_POINT('Ctrl Pts',(-25.7830427091458,21.1946349171485,-53.7783117506642));
#15980=CARTESIAN_POINT('Ctrl Pts',(-26.0481697824471,21.477879923486,-53.7987948838381));
#15981=CARTESIAN_POINT('Ctrl Pts',(-26.2679270647295,21.8179820977463,-53.823288773705));
#15982=CARTESIAN_POINT('Ctrl Pts',(-26.2786002779706,21.8348417146096,-53.8245014647242));
#15983=CARTESIAN_POINT('Ctrl Pts',(-26.2923840237608,21.857068875624,-53.8260986479468));
#15984=CARTESIAN_POINT('Ctrl Pts',(-26.295636757774,21.8623480725172,-53.8264778799225));
#15985=CARTESIAN_POINT('Ctrl Pts',(-26.3006343591503,21.8705118579788,-53.8270641595052));
#15986=CARTESIAN_POINT('Ctrl Pts',(-26.3023899826332,21.8733898722208,-53.8272708111726));
#15987=CARTESIAN_POINT('Ctrl Pts',(-26.3058778927084,21.8791278766723,-53.8276827591651));
#15988=CARTESIAN_POINT('Ctrl Pts',(-26.3076102506747,21.8819878187868,-53.8278880525357));
#15989=CARTESIAN_POINT('Ctrl Pts',(-26.3114417696561,21.8883355284416,-53.8283436418372));
#15990=CARTESIAN_POINT('Ctrl Pts',(-26.3135387770174,21.8918245833945,-53.8285940162184));
#15991=CARTESIAN_POINT('Ctrl Pts',(-26.3195735343807,21.9019085912587,-53.8293175262966));
#15992=CARTESIAN_POINT('Ctrl Pts',(-26.3234943044758,21.9085136273756,-53.8297912812035));
#15993=CARTESIAN_POINT('Ctrl Pts',(-26.3498570823684,21.9532889936326,-53.8330019621775));
#15994=CARTESIAN_POINT('Ctrl Pts',(-26.371533048071,21.9919027267853,-53.8357665455221));
#15995=CARTESIAN_POINT('Ctrl Pts',(-26.4162332703386,22.0755232163435,-53.8417481619889));
#15996=CARTESIAN_POINT('Ctrl Pts',(-26.4390077226515,22.1206493918931,-53.8449730416554));
#15997=CARTESIAN_POINT('Ctrl Pts',(-26.5041758098438,22.2576972187417,-53.8547596721978));
#15998=CARTESIAN_POINT('Ctrl Pts',(-26.5433071003439,22.3510931518908,-53.861421539032));
#15999=CARTESIAN_POINT('Ctrl Pts',(-26.6722433689188,22.7046744483083,-53.8865409505672));
#16000=CARTESIAN_POINT('Ctrl Pts',(-26.7330131296374,22.9741774182669,-53.9055964789788));
#16001=CARTESIAN_POINT('Ctrl Pts',(-26.7598832959582,23.2595305461044,-53.9240967512976));
#16002=CARTESIAN_POINT('Ctrl Pts',(-26.7608968990714,23.2709468391368,-53.924833956984));
#16003=CARTESIAN_POINT('Ctrl Pts',(-26.76244427627,23.2894979688374,-53.9260268554759));
#16004=CARTESIAN_POINT('Ctrl Pts',(-26.7630152225191,23.2966295035031,-53.9264842283835));
#16005=CARTESIAN_POINT('Ctrl Pts',(-26.7639816365523,23.3092279579645,-53.9272900142447));
#16006=CARTESIAN_POINT('Ctrl Pts',(-26.7643869122515,23.3146940692898,-53.9276388903131));
#16007=CARTESIAN_POINT('Ctrl Pts',(-26.7662605537946,23.3408700649972,-53.9293059945067));
#16008=CARTESIAN_POINT('Ctrl Pts',(-26.767542758271,23.3615934000929,-53.9306150855915));
#16009=CARTESIAN_POINT('Ctrl Pts',(-26.7688284710982,23.3862348875533,-53.932157775011));
#16010=CARTESIAN_POINT('Ctrl Pts',(-26.7690251912368,23.3901418453975,-53.9324019562176));
#16011=CARTESIAN_POINT('Ctrl Pts',(-26.7693323520063,23.3964716641396,-53.9327968805583));
#16012=CARTESIAN_POINT('Ctrl Pts',(-26.769447171445,23.3988942935331,-53.9329478689265));
#16013=CARTESIAN_POINT('Ctrl Pts',(-26.76964305871,23.4031284842292,-53.933211475259));
#16014=CARTESIAN_POINT('Ctrl Pts',(-26.7697253323798,23.4049399840895,-53.9333241615068));
#16015=CARTESIAN_POINT('Ctrl Pts',(-26.7698839076654,23.4084977414733,-53.9335452949049));
#16016=CARTESIAN_POINT('Ctrl Pts',(-26.7699603173148,23.4102439857482,-53.9336537479536));
#16017=CARTESIAN_POINT('Ctrl Pts',(-26.7701224129934,23.4140187899975,-53.9338880050728));
#16018=CARTESIAN_POINT('Ctrl Pts',(-26.7702076028248,23.4160473722205,-53.9340137810181));
#16019=CARTESIAN_POINT('Ctrl Pts',(-26.7704095782857,23.4209678291189,-53.9343185851533));
#16020=CARTESIAN_POINT('Ctrl Pts',(-26.7705243857482,23.4238597899097,-53.9344975023083));
#16021=CARTESIAN_POINT('Ctrl Pts',(-26.7708258853175,23.4317216455153,-53.9349832789564));
#16022=CARTESIAN_POINT('Ctrl Pts',(-26.7710049700657,23.4366918494909,-53.9352897169584));
#16023=CARTESIAN_POINT('Ctrl Pts',(-26.7723804683151,23.477490891901,-53.937799860012));
#16024=CARTESIAN_POINT('Ctrl Pts',(-26.7729905408346,23.5133385236836,-53.9399716842124));
#16025=CARTESIAN_POINT('Ctrl Pts',(-26.7730023566686,23.5491903981972,-53.9421167188325));
#16026=CARTESIAN_POINT('Ctrl Pts',(-26.7730023556334,23.5491872617795,-53.942116531179));
#16027=CARTESIAN_POINT('Ctrl Pts',(-26.7730945560227,23.8281201261137,-53.9588052287378));
#16028=CARTESIAN_POINT('Ctrl Pts',(-26.7369744698146,24.1059428445382,-53.9738720656566));
#16029=CARTESIAN_POINT('Ctrl Pts',(-26.6187707521688,24.552051586306,-53.9999189007627));
#16030=CARTESIAN_POINT('Ctrl Pts',(-26.5571558436671,24.7241023836079,-54.0104424369143));
#16031=CARTESIAN_POINT('Ctrl Pts',(-26.4738354566922,24.9063885917255,-54.0225828338893));
#16032=CARTESIAN_POINT('Ctrl Pts',(-26.4662088341052,24.9227105290593,-54.023678744104));
#16033=CARTESIAN_POINT('Ctrl Pts',(-26.4559781523645,24.9441352297471,-54.0251292783573));
#16034=CARTESIAN_POINT('Ctrl Pts',(-26.4534966669611,24.9492964369809,-54.0254796359503));
#16035=CARTESIAN_POINT('Ctrl Pts',(-26.4494155114942,24.9577271593998,-54.0260534614175));
#16036=CARTESIAN_POINT('Ctrl Pts',(-26.4478240284401,24.961000642503,-54.0262766433599));
#16037=CARTESIAN_POINT('Ctrl Pts',(-26.4447405262859,24.9673157940636,-54.0267079336213));
#16038=CARTESIAN_POINT('Ctrl Pts',(-26.443249249135,24.9703578211461,-54.0269160157792));
#16039=CARTESIAN_POINT('Ctrl Pts',(-26.4398110887038,24.9773433661698,-54.0273946023057));
#16040=CARTESIAN_POINT('Ctrl Pts',(-26.4378609275962,24.9812852552338,-54.0276652212466));
#16041=CARTESIAN_POINT('Ctrl Pts',(-26.4316554842877,24.9937640744431,-54.0285236909451));
#16042=CARTESIAN_POINT('Ctrl Pts',(-26.4273703959059,25.0022860511279,-54.0291125873443));
#16043=CARTESIAN_POINT('Ctrl Pts',(-26.4110843977381,25.0343197196009,-54.0313362557893));
#16044=CARTESIAN_POINT('Ctrl Pts',(-26.3988328610272,25.0577021741146,-54.0329798485356));
#16045=CARTESIAN_POINT('Ctrl Pts',(-26.3833746885691,25.0863430989516,-54.0350189574913));
#16046=CARTESIAN_POINT('Ctrl Pts',(-26.3804381510721,25.0917468539716,-54.0354048280166));
#16047=CARTESIAN_POINT('Ctrl Pts',(-26.3741996030749,25.1031489816459,-54.0362214649155));
#16048=CARTESIAN_POINT('Ctrl Pts',(-26.3708939116635,25.1091452960216,-54.0366523603786));
#16049=CARTESIAN_POINT('Ctrl Pts',(-26.3666905475507,25.1167127895278,-54.0371979788459));
#16050=CARTESIAN_POINT('Ctrl Pts',(-26.3658106081822,25.118293843151,-54.0373120738645));
#16051=CARTESIAN_POINT('Ctrl Pts',(-26.3636312476271,25.1222019159815,-54.0375943447815));
#16052=CARTESIAN_POINT('Ctrl Pts',(-26.3623302720827,25.1245280628413,-54.0377625755402));
#16053=CARTESIAN_POINT('Ctrl Pts',(-26.3576530459204,25.1328666551794,-54.0383664219273));
#16054=CARTESIAN_POINT('Ctrl Pts',(-26.354260404153,25.1388698427979,-54.0388026151492));
#16055=CARTESIAN_POINT('Ctrl Pts',(-26.3482420857702,25.1494397523406,-54.039573226755));
#16056=CARTESIAN_POINT('Ctrl Pts',(-26.3456244212331,25.1540110266204,-54.0399073623416));
#16057=CARTESIAN_POINT('Ctrl Pts',(-26.3409964033775,25.1620472619889,-54.0404962890854));
#16058=CARTESIAN_POINT('Ctrl Pts',(-26.3389907700402,25.1655149400047,-54.0407509144807));
#16059=CARTESIAN_POINT('Ctrl Pts',(-26.3347887704748,25.1727489127244,-54.0412831393293));
#16060=CARTESIAN_POINT('Ctrl Pts',(-26.3325912175981,25.1765145057206,-54.041560779806));
#16061=CARTESIAN_POINT('Ctrl Pts',(-26.3200151500943,25.1979639852111,-54.0431456668619));
#16062=CARTESIAN_POINT('Ctrl Pts',(-26.3094758783938,25.2155526515351,-54.0444584802907));
#16063=CARTESIAN_POINT('Ctrl Pts',(-26.1413332266607,25.4901822039067,-54.0651655423998));
#16064=CARTESIAN_POINT('Ctrl Pts',(-25.9486007724376,25.7239337604452,-54.0858881766233));
#16065=CARTESIAN_POINT('Ctrl Pts',(-25.6619031058536,25.9863692923315,-54.1118916215496));
#16066=CARTESIAN_POINT('Ctrl Pts',(-25.5951604670809,26.0426584064178,-54.1176578634111));
#16067=CARTESIAN_POINT('Ctrl Pts',(-25.505664169124,26.1121189027979,-54.1249462919421));
#16068=CARTESIAN_POINT('Ctrl Pts',(-25.4849252862279,26.1278163827829,-54.1266057840618));
#16069=CARTESIAN_POINT('Ctrl Pts',(-25.4561958483418,26.1490198674835,-54.1288620410255));
#16070=CARTESIAN_POINT('Ctrl Pts',(-25.448367725862,26.1547429438666,-54.1294725425885));
#16071=CARTESIAN_POINT('Ctrl Pts',(-25.4367182565902,26.1631793566274,-54.1303745936406));
#16072=CARTESIAN_POINT('Ctrl Pts',(-25.4329167182444,26.1659197668364,-54.1306679419268));
#16073=CARTESIAN_POINT('Ctrl Pts',(-25.4268531857238,26.1702707106203,-54.1311342059666));
#16074=CARTESIAN_POINT('Ctrl Pts',(-25.4245950823499,26.1718866166777,-54.1313074867353));
#16075=CARTESIAN_POINT('Ctrl Pts',(-25.4203032862934,26.1749494603274,-54.1316361414455));
#16076=CARTESIAN_POINT('Ctrl Pts',(-25.4182699974343,26.1763969564632,-54.1317915537984));
#16077=CARTESIAN_POINT('Ctrl Pts',(-25.4147179571499,26.1789194375477,-54.132062538667));
#16078=CARTESIAN_POINT('Ctrl Pts',(-25.4131999545484,26.1799954705384,-54.1321781841369));
#16079=CARTESIAN_POINT('Ctrl Pts',(-25.4102319034212,26.1820955077152,-54.1324039790384));
#16080=CARTESIAN_POINT('Ctrl Pts',(-25.408781944119,26.1831196261127,-54.1325141365193));
#16081=CARTESIAN_POINT('Ctrl Pts',(-25.4053208655009,26.1855599311382,-54.1327767325428));
#16082=CARTESIAN_POINT('Ctrl Pts',(-25.4033089659669,26.1869750169306,-54.1329290946841));
#16083=CARTESIAN_POINT('Ctrl Pts',(-25.3972284518379,26.1912413988257,-54.1333887275581));
#16084=CARTESIAN_POINT('Ctrl Pts',(-25.393154837788,26.1940856082853,-54.1336955126422));
#16085=CARTESIAN_POINT('Ctrl Pts',(-25.3518058090543,26.2228136207685,-54.1367981246812));
#16086=CARTESIAN_POINT('Ctrl Pts',(-25.3139918749871,26.2479183803324,-54.1395418231498));
#16087=CARTESIAN_POINT('Ctrl Pts',(-25.1961251910126,26.3226319838297,-54.1478513766108));
#16088=CARTESIAN_POINT('Ctrl Pts',(-25.1144142767542,26.3695406639125,-54.1532775352055));
#16089=CARTESIAN_POINT('Ctrl Pts',(-24.958764310648,26.4500425290349,-54.1632233292736));
#16090=CARTESIAN_POINT('Ctrl Pts',(-24.8853876011128,26.4845501442545,-54.1677602780092));
#16091=CARTESIAN_POINT('Ctrl Pts',(-24.6491029420874,26.5849697379848,-54.1821103432062));
#16092=CARTESIAN_POINT('Ctrl Pts',(-24.4820774102794,26.6403460727273,-54.191892514863));
#16093=CARTESIAN_POINT('Ctrl Pts',(-24.2353059855947,26.7003237651233,-54.2065893842924));
#16094=CARTESIAN_POINT('Ctrl Pts',(-24.1585864286003,26.7160344993569,-54.2111881145551));
#16095=CARTESIAN_POINT('Ctrl Pts',(-24.0421789256471,26.7354848961182,-54.2182535585527));
#16096=CARTESIAN_POINT('Ctrl Pts',(-24.0028664212789,26.7413083512809,-54.2206543829996));
#16097=CARTESIAN_POINT('Ctrl Pts',(-23.9560653553474,26.7473588910429,-54.223533099852));
#16098=CARTESIAN_POINT('Ctrl Pts',(-23.9486698859282,26.7482889184793,-54.2239885981075));
#16099=CARTESIAN_POINT('Ctrl Pts',(-23.9372789140357,26.7496812805819,-54.2246911394828));
#16100=CARTESIAN_POINT('Ctrl Pts',(-23.9332856271383,26.7501618096893,-54.2249376069083));
#16101=CARTESIAN_POINT('Ctrl Pts',(-23.9260042192606,26.7510241869914,-54.2253873511894));
#16102=CARTESIAN_POINT('Ctrl Pts',(-23.9227163849817,26.7514084475982,-54.2255905514854));
#16103=CARTESIAN_POINT('Ctrl Pts',(-23.9160573226146,26.752176317452,-54.2260023585802));
#16104=CARTESIAN_POINT('Ctrl Pts',(-23.9126860696489,26.7525596695694,-54.2262109732305));
#16105=CARTESIAN_POINT('Ctrl Pts',(-23.9030447207589,26.7536405872707,-54.2268079620533));
#16106=CARTESIAN_POINT('Ctrl Pts',(-23.8967731992431,26.7543250635403,-54.2271967491555));
#16107=CARTESIAN_POINT('Ctrl Pts',(-23.8697651641498,26.7571925076086,-54.2288730411456));
#16108=CARTESIAN_POINT('Ctrl Pts',(-23.8490101129141,26.7591925757223,-54.2301663035805));
#16109=CARTESIAN_POINT('Ctrl Pts',(-23.4731451342962,26.7917348749944,-54.2536824429032));
#16110=CARTESIAN_POINT('Ctrl Pts',(-23.1154739095442,26.7633479180483,-54.2780179244678));
#16111=CARTESIAN_POINT('Ctrl Pts',(-22.7078945038185,26.6616233102381,-54.3062288726731));
#16112=CARTESIAN_POINT('Ctrl Pts',(-22.6464090862336,26.6443215298324,-54.3104856719587));
#16113=CARTESIAN_POINT('Ctrl Pts',(-22.5357189712163,26.6095921115149,-54.3181074534668));
#16114=CARTESIAN_POINT('Ctrl Pts',(-22.486345273698,26.5927743535008,-54.321491678926));
#16115=CARTESIAN_POINT('Ctrl Pts',(-22.4214531628953,26.5688976294274,-54.3258995684854));
#16116=CARTESIAN_POINT('Ctrl Pts',(-22.4055539869589,26.5629044384984,-54.326976302491));
#16117=CARTESIAN_POINT('Ctrl Pts',(-22.383090840696,26.5542334534166,-54.3284922130084));
#16118=CARTESIAN_POINT('Ctrl Pts',(-22.3764874835089,26.5516594359448,-54.3289371769255));
#16119=CARTESIAN_POINT('Ctrl Pts',(-22.3664243993078,26.5476985124281,-54.3296142064318));
#16120=CARTESIAN_POINT('Ctrl Pts',(-22.3629585500161,26.5463273731909,-54.3298471901444));
#16121=CARTESIAN_POINT('Ctrl Pts',(-22.3565533634135,26.5437805305491,-54.330277395391));
#16122=CARTESIAN_POINT('Ctrl Pts',(-22.3536133701421,26.5426065049949,-54.3304747165546));
#16123=CARTESIAN_POINT('Ctrl Pts',(-22.3488160018605,26.5406825742445,-54.3307964569059));
#16124=CARTESIAN_POINT('Ctrl Pts',(-22.3469575966116,26.5399352696889,-54.3309210336652));
#16125=CARTESIAN_POINT('Ctrl Pts',(-22.3433927340596,26.5384978997172,-54.3311598863868));
#16126=CARTESIAN_POINT('Ctrl Pts',(-22.3416861760813,26.5378081068679,-54.3312741782128));
#16127=CARTESIAN_POINT('Ctrl Pts',(-22.3377198094814,26.5362009418886,-54.3315396975375));
#16128=CARTESIAN_POINT('Ctrl Pts',(-22.3354604448534,26.5352824639767,-54.3316908574796));
#16129=CARTESIAN_POINT('Ctrl Pts',(-22.328329516505,26.5323741588045,-54.3321676717003));
#16130=CARTESIAN_POINT('Ctrl Pts',(-22.3234617507009,26.5303749510802,-54.332492757533));
#16131=CARTESIAN_POINT('Ctrl Pts',(-22.2831771906318,26.5137145171572,-54.3351799488851));
#16132=CARTESIAN_POINT('Ctrl Pts',(-22.2480177698886,26.4984336323821,-54.3375050894075));
#16133=CARTESIAN_POINT('Ctrl Pts',(-22.1665638548763,26.4612907218669,-54.3428631936693));
#16134=CARTESIAN_POINT('Ctrl Pts',(-22.1205172681142,26.4389531945934,-54.3458702400929));
#16135=CARTESIAN_POINT('Ctrl Pts',(-22.0750359442814,26.415536737968,-54.34883718749));
#16136=CARTESIAN_POINT('Ctrl Pts',(-22.0750360179885,26.4155367759168,-54.5955012513333));
#16137=CARTESIAN_POINT('Ctrl Pts',(-22.1009742172714,26.4288912834129,-54.5936150694628));
#16138=CARTESIAN_POINT('Ctrl Pts',(-22.1270929863428,26.4418931842608,-54.5917178026719));
#16139=CARTESIAN_POINT('Ctrl Pts',(-22.3631894087763,26.5554478916475,-54.5745881662261));
#16140=CARTESIAN_POINT('Ctrl Pts',(-22.583295460347,26.6333174528364,-54.5586903844263));
#16141=CARTESIAN_POINT('Ctrl Pts',(-22.9444643185385,26.7185761671403,-54.533710942971));
#16142=CARTESIAN_POINT('Ctrl Pts',(-23.0810228472947,26.7416608412576,-54.5245232806531));
#16143=CARTESIAN_POINT('Ctrl Pts',(-23.2342690244468,26.7575127830412,-54.5147800949232));
#16144=CARTESIAN_POINT('Ctrl Pts',(-23.2498927320136,26.7590136495353,-54.5137933323343));
#16145=CARTESIAN_POINT('Ctrl Pts',(-23.26924961122,26.7607305158691,-54.512579441191));
#16146=CARTESIAN_POINT('Ctrl Pts',(-23.2729726611281,26.761054207585,-54.5123463605135));
#16147=CARTESIAN_POINT('Ctrl Pts',(-23.278836856725,26.76155378028,-54.5119798662717));
#16148=CARTESIAN_POINT('Ctrl Pts',(-23.2809776147187,26.7617339962119,-54.5118462081358));
#16149=CARTESIAN_POINT('Ctrl Pts',(-23.2849790632726,26.7620668219165,-54.5115966278497));
#16150=CARTESIAN_POINT('Ctrl Pts',(-23.2868396937196,26.7622199544339,-54.5114806769453));
#16151=CARTESIAN_POINT('Ctrl Pts',(-23.2910168387963,26.7625600853323,-54.511220591711));
#16152=CARTESIAN_POINT('Ctrl Pts',(-23.2933334182414,26.7627461943912,-54.5110765085364));
#16153=CARTESIAN_POINT('Ctrl Pts',(-23.2992212851966,26.7632128035431,-54.5107106956386));
#16154=CARTESIAN_POINT('Ctrl Pts',(-23.3027928534128,26.7634898561237,-54.5104891606409));
#16155=CARTESIAN_POINT('Ctrl Pts',(-23.3224780566783,26.7649838549102,-54.5092701214903));
#16156=CARTESIAN_POINT('Ctrl Pts',(-23.3386005835814,26.7660855762527,-54.5082790254939));
#16157=CARTESIAN_POINT('Ctrl Pts',(-23.6681943649612,26.7861186447997,-54.4881550361072));
#16158=CARTESIAN_POINT('Ctrl Pts',(-23.9828179903954,26.7592561360464,-54.4713535661549));
#16159=CARTESIAN_POINT('Ctrl Pts',(-24.4493290146231,26.6494516703908,-54.4442368782231));
#16160=CARTESIAN_POINT('Ctrl Pts',(-24.6068665806205,26.5993392031658,-54.4346940865865));
#16161=CARTESIAN_POINT('Ctrl Pts',(-24.7744372900431,26.5314832468387,-54.4237802596548));
#16162=CARTESIAN_POINT('Ctrl Pts',(-24.7889708301596,26.5254738449781,-54.4228273463262));
#16163=CARTESIAN_POINT('Ctrl Pts',(-24.8106793615006,26.516311057799,-54.4213942194191));
#16164=CARTESIAN_POINT('Ctrl Pts',(-24.8178879262136,26.5132374250804,-54.4209167087605));
#16165=CARTESIAN_POINT('Ctrl Pts',(-24.8294509112932,26.5082572077584,-54.4201481097848));
#16166=CARTESIAN_POINT('Ctrl Pts',(-24.8338124793116,26.5063672145977,-54.4198575875126));
#16167=CARTESIAN_POINT('Ctrl Pts',(-24.8421309194249,26.5027407139094,-54.4193023343973));
#16168=CARTESIAN_POINT('Ctrl Pts',(-24.8460885146703,26.5010058829152,-54.419037661354));
#16169=CARTESIAN_POINT('Ctrl Pts',(-24.8530782774275,26.4979251126218,-54.4185693073353));
#16170=CARTESIAN_POINT('Ctrl Pts',(-24.8561118843654,26.4965824383757,-54.4183657386683));
#16171=CARTESIAN_POINT('Ctrl Pts',(-24.8620710026045,26.4939339216791,-54.4179652632655));
#16172=CARTESIAN_POINT('Ctrl Pts',(-24.8649966513385,26.4926283958728,-54.4177683675933));
#16173=CARTESIAN_POINT('Ctrl Pts',(-24.8719997821465,26.4894908259995,-54.4172963822152));
#16174=CARTESIAN_POINT('Ctrl Pts',(-24.8760754010203,26.4876546600464,-54.4170211507328));
#16175=CARTESIAN_POINT('Ctrl Pts',(-24.8884585096692,26.4820447444417,-54.416183223067));
#16176=CARTESIAN_POINT('Ctrl Pts',(-24.8967537509843,26.4782442123375,-54.4156196032885));
#16177=CARTESIAN_POINT('Ctrl Pts',(-24.9282734109128,26.4636409527045,-54.4134691265685));
#16178=CARTESIAN_POINT('Ctrl Pts',(-24.9513843929305,26.4525969429495,-54.4118739284959));
#16179=CARTESIAN_POINT('Ctrl Pts',(-24.9797939940123,26.43860248508,-54.4098896485956));
#16180=CARTESIAN_POINT('Ctrl Pts',(-24.9852196508811,26.4359107948562,-54.4095096297131));
#16181=CARTESIAN_POINT('Ctrl Pts',(-24.9967707431323,26.4301396181388,-54.4086983040156));
#16182=CARTESIAN_POINT('Ctrl Pts',(-25.0028939959815,26.4270558516583,-54.4082668498435));
#16183=CARTESIAN_POINT('Ctrl Pts',(-25.0100883018596,26.4234038601594,-54.4077583082061));
#16184=CARTESIAN_POINT('Ctrl Pts',(-25.0111689686063,26.4228545223064,-54.4076818763637));
#16185=CARTESIAN_POINT('Ctrl Pts',(-25.0150691686775,26.420869154386,-54.4074058729279));
#16186=CARTESIAN_POINT('Ctrl Pts',(-25.0178868897647,26.4194295853725,-54.4072061788152));
#16187=CARTESIAN_POINT('Ctrl Pts',(-25.0268295150917,26.4148441928803,-54.4065714724517));
#16188=CARTESIAN_POINT('Ctrl Pts',(-25.0329464293589,26.4116829044076,-54.4061359262017));
#16189=CARTESIAN_POINT('Ctrl Pts',(-25.0438219120351,26.4060180997954,-54.4053590563451));
#16190=CARTESIAN_POINT('Ctrl Pts',(-25.0485844490868,26.4035222242766,-54.4050179971229));
#16191=CARTESIAN_POINT('Ctrl Pts',(-25.0568830071811,26.3991467398329,-54.4044222146683));
#16192=CARTESIAN_POINT('Ctrl Pts',(-25.0604218225257,26.3972724318059,-54.4041676737734));
#16193=CARTESIAN_POINT('Ctrl Pts',(-25.0678161920721,26.3933383916417,-54.40363480983));
#16194=CARTESIAN_POINT('Ctrl Pts',(-25.0716710651511,26.3912774024211,-54.403356444221));
#16195=CARTESIAN_POINT('Ctrl Pts',(-25.0918412915703,26.3804406637514,-54.4018969327223));
#16196=CARTESIAN_POINT('Ctrl Pts',(-25.1080846864529,26.3715323339636,-54.4007112912739));
#16197=CARTESIAN_POINT('Ctrl Pts',(-25.1733925527948,26.3349797233172,-54.3959025549334));
#16198=CARTESIAN_POINT('Ctrl Pts',(-25.2218031739475,26.3061928297383,-54.3922417445337));
#16199=CARTESIAN_POINT('Ctrl Pts',(-25.3760985920768,26.2088813007158,-54.3802628235232));
#16200=CARTESIAN_POINT('Ctrl Pts',(-25.4787161511149,26.1354110209033,-54.3718012654041));
#16201=CARTESIAN_POINT('Ctrl Pts',(-25.6625980719657,25.9867051271226,-54.3558168687769));
#16202=CARTESIAN_POINT('Ctrl Pts',(-25.7448147438841,25.9129209826296,-54.3483199165899));
#16203=CARTESIAN_POINT('Ctrl Pts',(-25.9185695814987,25.7400771179663,-54.3318795414821));
#16204=CARTESIAN_POINT('Ctrl Pts',(-26.0080210667679,25.6391855312603,-54.3229954344297));
#16205=CARTESIAN_POINT('Ctrl Pts',(-26.0944882661496,25.5283870092592,-54.3141920366693));
#16206=CARTESIAN_POINT('Ctrl Pts',(-26.0980590574081,25.5237857573089,-54.3138280785755));
#16207=CARTESIAN_POINT('Ctrl Pts',(-26.1031876666514,25.5171400133166,-54.3133047775727));
#16208=CARTESIAN_POINT('Ctrl Pts',(-26.1047555165223,25.5151033324617,-54.3131447250498));
#16209=CARTESIAN_POINT('Ctrl Pts',(-26.1074773118739,25.5115588797814,-54.3128667440592));
#16210=CARTESIAN_POINT('Ctrl Pts',(-26.1086323628434,25.5100519620076,-54.3127487364862));
#16211=CARTESIAN_POINT('Ctrl Pts',(-26.110864918976,25.5071339580292,-54.3125205666545));
#16212=CARTESIAN_POINT('Ctrl Pts',(-26.1119425871162,25.5057230056791,-54.3124103925851));
#16213=CARTESIAN_POINT('Ctrl Pts',(-26.1145109616175,25.5023545579807,-54.3121477321574));
#16214=CARTESIAN_POINT('Ctrl Pts',(-26.1160005959615,25.5003962410827,-54.3119953222756));
#16215=CARTESIAN_POINT('Ctrl Pts',(-26.1204930444195,25.494476279275,-54.3115354678894));
#16216=CARTESIAN_POINT('Ctrl Pts',(-26.1234889543977,25.4905093671582,-54.3112285096602));
#16217=CARTESIAN_POINT('Ctrl Pts',(-26.153790717227,25.4501928925878,-54.3081206674394));
#16218=CARTESIAN_POINT('Ctrl Pts',(-26.180335379242,25.4132740538922,-54.3053721020731));
#16219=CARTESIAN_POINT('Ctrl Pts',(-26.2081617694405,25.3727918051171,-54.3024472332834));
#16220=CARTESIAN_POINT('Ctrl Pts',(-26.2102268809981,25.3697764750768,-54.3022298981055));
#16221=CARTESIAN_POINT('Ctrl Pts',(-26.2227654635382,25.3514015542697,-54.3009086392474));
#16222=CARTESIAN_POINT('Ctrl Pts',(-26.2331112055474,25.3359547848174,-54.2998112867053));
#16223=CARTESIAN_POINT('Ctrl Pts',(-26.4171144503833,25.0560185839087,-54.2801471847028));
#16224=CARTESIAN_POINT('Ctrl Pts',(-26.5510373795378,24.7674481398338,-54.2632735533612));
#16225=CARTESIAN_POINT('Ctrl Pts',(-26.673141057891,24.3544453302687,-54.2384679291315));
#16226=CARTESIAN_POINT('Ctrl Pts',(-26.6996713705618,24.2433004487383,-54.2317531786716));
#16227=CARTESIAN_POINT('Ctrl Pts',(-26.7237305968523,24.1119716651996,-54.2236720722379));
#16228=CARTESIAN_POINT('Ctrl Pts',(-26.7270435125599,24.0929222779478,-54.2224964523209));
#16229=CARTESIAN_POINT('Ctrl Pts',(-26.7311400711194,24.0680426424433,-54.2209561776751));
#16230=CARTESIAN_POINT('Ctrl Pts',(-26.7320794992369,24.0622381615255,-54.2205964849776));
#16231=CARTESIAN_POINT('Ctrl Pts',(-26.7335801070785,24.0528026382245,-54.2200112155008));
#16232=CARTESIAN_POINT('Ctrl Pts',(-26.7341509748491,24.0491731318642,-54.2197859469785));
#16233=CARTESIAN_POINT('Ctrl Pts',(-26.7352345918202,24.0422060271325,-54.2193532626609));
#16234=CARTESIAN_POINT('Ctrl Pts',(-26.7357483048037,24.0388685817391,-54.2191458777921));
#16235=CARTESIAN_POINT('Ctrl Pts',(-26.736907822635,24.0312559758834,-54.2186725711534));
#16236=CARTESIAN_POINT('Ctrl Pts',(-26.7375502703133,24.0269803174432,-54.2184065431678));
#16237=CARTESIAN_POINT('Ctrl Pts',(-26.7395252783619,24.0136536606325,-54.2175767608807));
#16238=CARTESIAN_POINT('Ctrl Pts',(-26.7408278952094,24.0045983316087,-54.2170120578741));
#16239=CARTESIAN_POINT('Ctrl Pts',(-26.7506445087164,23.9342320601815,-54.2126169664548));
#16240=CARTESIAN_POINT('Ctrl Pts',(-26.757428561916,23.8726965365977,-54.208732104771));
#16241=CARTESIAN_POINT('Ctrl Pts',(-26.7628422223502,23.8060067312011,-54.2044730553834));
#16242=CARTESIAN_POINT('Ctrl Pts',(-26.7632364584641,23.8010054318586,-54.2041533613094));
#16243=CARTESIAN_POINT('Ctrl Pts',(-26.7652813814413,23.7742666012615,-54.2024425852595));
#16244=CARTESIAN_POINT('Ctrl Pts',(-26.7667231196907,23.7525140664367,-54.2010452825869));
#16245=CARTESIAN_POINT('Ctrl Pts',(-26.7713625741982,23.6698069936096,-54.1957113297201));
#16246=CARTESIAN_POINT('Ctrl Pts',(-26.7730489237305,23.608783393372,-54.191731846219));
#16247=CARTESIAN_POINT('Ctrl Pts',(-26.7728714384885,23.3800730712408,-54.1766626127112));
#16248=CARTESIAN_POINT('Ctrl Pts',(-26.7596550822314,23.2126720043107,-54.1653045718704));
#16249=CARTESIAN_POINT('Ctrl Pts',(-26.7044156726278,22.8632142067214,-54.1413667466472));
#16250=CARTESIAN_POINT('Ctrl Pts',(-26.6594738075372,22.6821927807123,-54.1288348467689));
#16251=CARTESIAN_POINT('Ctrl Pts',(-26.5954450045766,22.4952402911739,-54.1163823865396));
#16252=CARTESIAN_POINT('Ctrl Pts',(-26.5916866645825,22.4844540286091,-54.1156657957847));
#16253=CARTESIAN_POINT('Ctrl Pts',(-26.5867052295387,22.4703984884452,-54.1147346490989));
#16254=CARTESIAN_POINT('Ctrl Pts',(-26.5855341190207,22.4671110696124,-54.114517054414));
#16255=CARTESIAN_POINT('Ctrl Pts',(-26.5837225009203,22.46205169625,-54.1141824724128));
#16256=CARTESIAN_POINT('Ctrl Pts',(-26.5830857800475,22.4602784034766,-54.114065259137));
#16257=CARTESIAN_POINT('Ctrl Pts',(-26.5818156108227,22.456750661972,-54.1138321922));
#16258=CARTESIAN_POINT('Ctrl Pts',(-26.5811821981013,22.4549962150516,-54.1137163377503));
#16259=CARTESIAN_POINT('Ctrl Pts',(-26.5797645641339,22.4510802545368,-54.113457873606));
#16260=CARTESIAN_POINT('Ctrl Pts',(-26.5789795544314,22.4489190347964,-54.1133153122197));
#16261=CARTESIAN_POINT('Ctrl Pts',(-26.5766734977941,22.4425913146826,-54.112898158414));
#16262=CARTESIAN_POINT('Ctrl Pts',(-26.5751461537557,22.4384270905879,-54.1126239428909));
#16263=CARTESIAN_POINT('Ctrl Pts',(-26.5638572334469,22.4078438864063,-54.1106122181435));
#16264=CARTESIAN_POINT('Ctrl Pts',(-26.5537579086593,22.3815496641164,-54.108894636067));
#16265=CARTESIAN_POINT('Ctrl Pts',(-26.5194848977408,22.2956977234904,-54.1033157277895));
#16266=CARTESIAN_POINT('Ctrl Pts',(-26.4938729247173,22.2367272127551,-54.0995299467616));
#16267=CARTESIAN_POINT('Ctrl Pts',(-26.4022312468814,22.0418944696496,-54.0870528538413));
#16268=CARTESIAN_POINT('Ctrl Pts',(-26.3284184467814,21.9099090050923,-54.0786453077253));
#16269=CARTESIAN_POINT('Ctrl Pts',(-26.1904272751789,21.6993796456838,-54.0645793114023));
#16270=CARTESIAN_POINT('Ctrl Pts',(-26.1313243030524,21.6178134821019,-54.0589486018106));
#16271=CARTESIAN_POINT('Ctrl Pts',(-26.0266007056092,21.486681368543,-54.0494138811664));
#16272=CARTESIAN_POINT('Ctrl Pts',(-25.9830712178427,21.4355377110349,-54.0455622084889));
#16273=CARTESIAN_POINT('Ctrl Pts',(-25.8707981564879,21.3116836032964,-54.0358364942848));
#16274=CARTESIAN_POINT('Ctrl Pts',(-25.8002108937413,21.2407488876991,-54.0298999361944));
#16275=CARTESIAN_POINT('Ctrl Pts',(-25.7195278272604,21.1668830254051,-54.0232418543762));
#16276=CARTESIAN_POINT('Ctrl Pts',(-25.7125831670454,21.160580643764,-54.0226697747992));
#16277=CARTESIAN_POINT('Ctrl Pts',(-25.702241333459,21.1512772702684,-54.0218192855807));
#16278=CARTESIAN_POINT('Ctrl Pts',(-25.6988651344784,21.1482529499561,-54.0215418603151));
#16279=CARTESIAN_POINT('Ctrl Pts',(-25.6930792016495,21.1430920058882,-54.0210668051702));
#16280=CARTESIAN_POINT('Ctrl Pts',(-25.6906726177405,21.1409518469296,-54.0208693240994));
#16281=CARTESIAN_POINT('Ctrl Pts',(-25.6859882413396,21.1367986204205,-54.0204851456695));
#16282=CARTESIAN_POINT('Ctrl Pts',(-25.6837108003061,21.1347851609165,-54.0202984650755));
#16283=CARTESIAN_POINT('Ctrl Pts',(-25.6782628262592,21.1299823853417,-54.019852130622));
#16284=CARTESIAN_POINT('Ctrl Pts',(-25.6750896590907,21.1271960781907,-54.0195923515127));
#16285=CARTESIAN_POINT('Ctrl Pts',(-25.6655808670747,21.1188796028594,-54.018814445408));
#16286=CARTESIAN_POINT('Ctrl Pts',(-25.6592290995492,21.1133680207615,-54.0182955464928));
#16287=CARTESIAN_POINT('Ctrl Pts',(-25.6043765924501,21.0661462599866,-54.0138205947588));
#16288=CARTESIAN_POINT('Ctrl Pts',(-25.5546685121085,21.0258664172482,-54.0098060901969));
#16289=CARTESIAN_POINT('Ctrl Pts',(-25.4250785415863,20.9270976951786,-53.9994302655898));
#16290=CARTESIAN_POINT('Ctrl Pts',(-25.3436445356265,20.8707645571461,-53.9929913648597));
#16291=CARTESIAN_POINT('Ctrl Pts',(-25.0177259591958,20.6668252481455,-53.9675615037369));
#16292=CARTESIAN_POINT('Ctrl Pts',(-24.756674184183,20.5482266875432,-53.9477671583786));
#16293=CARTESIAN_POINT('Ctrl Pts',(-24.4769079329637,20.4635919133481,-53.9286710824796));
#16294=CARTESIAN_POINT('Ctrl Pts',(-24.4703786773796,20.4616392695661,-53.9282266201795));
#16295=CARTESIAN_POINT('Ctrl Pts',(-24.4632035835527,20.4595182525449,-53.9277395528156));
#16296=CARTESIAN_POINT('Ctrl Pts',(-24.4625638782925,20.4593293663158,-53.9276961395058));
#16297=CARTESIAN_POINT('Ctrl Pts',(-24.4532336303569,20.4565775662185,-53.9270631195816));
#16298=CARTESIAN_POINT('Ctrl Pts',(-24.4445322824664,20.4540510867884,-53.9264749585841));
#16299=CARTESIAN_POINT('Ctrl Pts',(-24.4345543327874,20.4511995117115,-53.9258030997667));
#16300=CARTESIAN_POINT('Ctrl Pts',(-24.4332881398974,20.4508384885672,-53.9257178892359));
#16301=CARTESIAN_POINT('Ctrl Pts',(-24.4252426810515,20.4485498581434,-53.9251767616788));
#16302=CARTESIAN_POINT('Ctrl Pts',(-24.4184572699734,20.4466437015135,-53.9247217579067));
#16303=CARTESIAN_POINT('Ctrl Pts',(-24.3731273895862,20.4340699314905,-53.9216915176154));
#16304=CARTESIAN_POINT('Ctrl Pts',(-24.3343912753339,20.424097732735,-53.9191473817995));
#16305=CARTESIAN_POINT('Ctrl Pts',(-24.2902953251472,20.4136169778787,-53.9163100795311));
#16306=CARTESIAN_POINT('Ctrl Pts',(-24.2851101449787,20.4123981337387,-53.915977362568));
#16307=CARTESIAN_POINT('Ctrl Pts',(-24.277534453801,20.4106371768667,-53.9154926168509));
#16308=CARTESIAN_POINT('Ctrl Pts',(-24.2751463429577,20.4100849353739,-53.9153400063549));
#16309=CARTESIAN_POINT('Ctrl Pts',(-24.2709622100026,20.4091223981143,-53.9150729711244));
#16310=CARTESIAN_POINT('Ctrl Pts',(-24.2691664648354,20.4087109175665,-53.9149584775118));
#16311=CARTESIAN_POINT('Ctrl Pts',(-24.2654231311523,20.4078565405154,-53.9147200445019));
#16312=CARTESIAN_POINT('Ctrl Pts',(-24.2634754872032,20.4074139154918,-53.9145961211379));
#16313=CARTESIAN_POINT('Ctrl Pts',(-24.2595002706259,20.4065143862533,-53.9143434568099));
#16314=CARTESIAN_POINT('Ctrl Pts',(-24.2574726644909,20.4060576321841,-53.9142147245971));
#16315=CARTESIAN_POINT('Ctrl Pts',(-24.2525061298565,20.4049438798658,-53.9138997455623));
#16316=CARTESIAN_POINT('Ctrl Pts',(-24.2495667123517,20.4042890372614,-53.9137136225797));
#16317=CARTESIAN_POINT('Ctrl Pts',(-24.2414884065767,20.4025012360297,-53.9132029082083));
#16318=CARTESIAN_POINT('Ctrl Pts',(-24.2363476263804,20.401376736106,-53.9128787959768));
#16319=CARTESIAN_POINT('Ctrl Pts',(-24.0503380479243,20.3611659413888,-53.9011828202846));
#16320=CARTESIAN_POINT('Ctrl Pts',(-23.866408765732,20.337710451219,-53.8906825218747));
#16321=CARTESIAN_POINT('Ctrl Pts',(-23.3713358513392,20.317538285856,-53.8628958954641));
#16322=CARTESIAN_POINT('Ctrl Pts',(-23.0610612513995,20.3497645498736,-53.8458092008685));
#16323=CARTESIAN_POINT('Ctrl Pts',(-22.7420104950499,20.4304426213078,-53.8258881001028));
#16324=CARTESIAN_POINT('Ctrl Pts',(-22.7238749286448,20.4351972993127,-53.8247481798572));
#16325=CARTESIAN_POINT('Ctrl Pts',(-22.6999441805584,20.4416950100567,-53.8232336485858));
#16326=CARTESIAN_POINT('Ctrl Pts',(-22.6941106933179,20.4432965762398,-53.8228636418414));
#16327=CARTESIAN_POINT('Ctrl Pts',(-22.6850626728558,20.4458080996332,-53.822288463435));
#16328=CARTESIAN_POINT('Ctrl Pts',(-22.68184496556,20.446706652778,-53.8220836635893));
#16329=CARTESIAN_POINT('Ctrl Pts',(-22.6754063218675,20.4485154579454,-53.8216733518423));
#16330=CARTESIAN_POINT('Ctrl Pts',(-22.672185394741,20.4494257276973,-53.8214678395778));
#16331=CARTESIAN_POINT('Ctrl Pts',(-22.6649988691765,20.451468814688,-53.821008730998));
#16332=CARTESIAN_POINT('Ctrl Pts',(-22.6610340206476,20.452604228361,-53.8207550501648));
#16333=CARTESIAN_POINT('Ctrl Pts',(-22.6494486487209,20.4559460072104,-53.8200126483842));
#16334=CARTESIAN_POINT('Ctrl Pts',(-22.6418341206175,20.4581728930602,-53.8195232570967));
#16335=CARTESIAN_POINT('Ctrl Pts',(-22.5862191318852,20.4746607855187,-53.8159381606937));
#16336=CARTESIAN_POINT('Ctrl Pts',(-22.5385509000267,20.4900100024995,-53.8128069140744));
#16337=CARTESIAN_POINT('Ctrl Pts',(-22.3844087746391,20.5436389051829,-53.8024819838771));
#16338=CARTESIAN_POINT('Ctrl Pts',(-22.2795990037145,20.5864117902428,-53.7951428469154));
#16339=CARTESIAN_POINT('Ctrl Pts',(-21.943420816368,20.7447191109677,-53.770568848282));
#16340=CARTESIAN_POINT('Ctrl Pts',(-21.7236990882241,20.8825547101724,-53.7527419670825));
#16341=CARTESIAN_POINT('Ctrl Pts',(-21.4524167307334,21.102109792908,-53.7296528279958));
#16342=CARTESIAN_POINT('Ctrl Pts',(-21.3844501649853,21.1620269118271,-53.7237720500036));
#16343=CARTESIAN_POINT('Ctrl Pts',(-21.3144569892859,21.2291801283998,-53.7176911851176));
#16344=CARTESIAN_POINT('Ctrl Pts',(-21.3098359272546,21.2336402963337,-53.7172895999336));
#16345=CARTESIAN_POINT('Ctrl Pts',(-21.3034494227692,21.2398414212685,-53.7167344699961));
#16346=CARTESIAN_POINT('Ctrl Pts',(-21.3016726499497,21.2415706079618,-53.7165800155729));
#16347=CARTESIAN_POINT('Ctrl Pts',(-21.2986233788433,21.2445450718343,-53.7163149234124));
#16348=CARTESIAN_POINT('Ctrl Pts',(-21.2973499173736,21.2457893528076,-53.7162042075203));
#16349=CARTESIAN_POINT('Ctrl Pts',(-21.2947498844039,21.2483340228526,-53.7159781474176));
#16350=CARTESIAN_POINT('Ctrl Pts',(-21.2934234087759,21.249634500981,-53.7158628112706));
#16351=CARTESIAN_POINT('Ctrl Pts',(-21.2903300971001,21.2526724367763,-53.7155938350396));
#16352=CARTESIAN_POINT('Ctrl Pts',(-21.2885641348045,21.2544107909772,-53.7154402658708));
#16353=CARTESIAN_POINT('Ctrl Pts',(-21.284841350213,21.258083839506,-53.7151165014098));
#16354=CARTESIAN_POINT('Ctrl Pts',(-21.2828849957527,21.2600190082909,-53.7149463436172));
#16355=CARTESIAN_POINT('Ctrl Pts',(-21.2776468026401,21.2652137665911,-53.7144906881227));
#16356=CARTESIAN_POINT('Ctrl Pts',(-21.2743694837242,21.2684779349518,-53.7142055472385));
#16357=CARTESIAN_POINT('Ctrl Pts',(-21.196941731958,21.3459277746352,-53.7074673264598));
#16358=CARTESIAN_POINT('Ctrl Pts',(-21.1264407299458,21.4236916997899,-53.701294987091));
#16359=CARTESIAN_POINT('Ctrl Pts',(-20.8112954570304,21.8073842075662,-53.672744741342));
#16360=CARTESIAN_POINT('Ctrl Pts',(-20.6199783799416,22.1527512741779,-53.6519673604469));
#16361=CARTESIAN_POINT('Ctrl Pts',(-20.4891070038943,22.5423442634338,-53.6270974871756));
#16362=CARTESIAN_POINT('Ctrl Pts',(-20.4831182953728,22.5607180094763,-53.6259227552702));
#16363=CARTESIAN_POINT('Ctrl Pts',(-20.4754502655289,22.584982581198,-53.6243686209678));
#16364=CARTESIAN_POINT('Ctrl Pts',(-20.473621887071,22.590826177515,-53.6239941311172));
#16365=CARTESIAN_POINT('Ctrl Pts',(-20.4708172786213,22.5998803177259,-53.6234135545696));
#16366=CARTESIAN_POINT('Ctrl Pts',(-20.4698293844633,22.6030872574051,-53.6232078513257));
#16367=CARTESIAN_POINT('Ctrl Pts',(-20.4679646195898,22.6091745038532,-53.6228172697673));
#16368=CARTESIAN_POINT('Ctrl Pts',(-20.4670867724079,22.6120545098145,-53.62263242373));
#16369=CARTESIAN_POINT('Ctrl Pts',(-20.4650656129891,22.6187189208838,-53.6222045591596));
#16370=CARTESIAN_POINT('Ctrl Pts',(-20.4639252275865,22.6225042020733,-53.6219614449882));
#16371=CARTESIAN_POINT('Ctrl Pts',(-20.4607459435362,22.6331279350019,-53.6212788549182));
#16372=CARTESIAN_POINT('Ctrl Pts',(-20.458722797967,22.6399710431983,-53.6208388639674));
#16373=CARTESIAN_POINT('Ctrl Pts',(-20.4471157125049,22.6797160134874,-53.618281517893));
#16374=CARTESIAN_POINT('Ctrl Pts',(-20.4380346299818,22.712761317348,-53.6161478099673));
#16375=CARTESIAN_POINT('Ctrl Pts',(-20.4133275438689,22.8086264552958,-53.6099338946471));
#16376=CARTESIAN_POINT('Ctrl Pts',(-20.3990657646876,22.8717773208185,-53.6058106594238));
#16377=CARTESIAN_POINT('Ctrl Pts',(-20.3491161911391,23.1287405978441,-53.5889063927086));
#16378=CARTESIAN_POINT('Ctrl Pts',(-20.3293407977036,23.3251866418383,-53.5756600584079));
#16379=CARTESIAN_POINT('Ctrl Pts',(-20.3260069066221,23.7079112193692,-53.5497530684138));
#16380=CARTESIAN_POINT('Ctrl Pts',(-20.3404482932774,23.8934516875078,-53.5371588048765));
#16381=CARTESIAN_POINT('Ctrl Pts',(-20.3763315967665,24.1101556323566,-53.5230678284819));
#16382=CARTESIAN_POINT('Ctrl Pts',(-20.3823938050241,24.1434952293927,-53.5209182514212));
#16383=CARTESIAN_POINT('Ctrl Pts',(-20.3899678458289,24.181714358312,-53.5184799692282));
#16384=CARTESIAN_POINT('Ctrl Pts',(-20.3909664742216,24.1866917998807,-53.5181629286902));
#16385=CARTESIAN_POINT('Ctrl Pts',(-20.3924552144743,24.1940222438682,-53.517696781677));
#16386=CARTESIAN_POINT('Ctrl Pts',(-20.3929361976369,24.1963770597373,-53.517547154681));
#16387=CARTESIAN_POINT('Ctrl Pts',(-20.3937866896582,24.2005173045439,-53.5172842886015));
#16388=CARTESIAN_POINT('Ctrl Pts',(-20.3941550794573,24.2023029582712,-53.5171709849542));
#16389=CARTESIAN_POINT('Ctrl Pts',(-20.3949340234267,24.2060625184211,-53.5169325774556));
#16390=CARTESIAN_POINT('Ctrl Pts',(-20.395344913707,24.2080363482531,-53.5168074935211));
#16391=CARTESIAN_POINT('Ctrl Pts',(-20.3964170680846,24.2131626358478,-53.516482849408));
#16392=CARTESIAN_POINT('Ctrl Pts',(-20.3970812086777,24.2163145000074,-53.5162834552192));
#16393=CARTESIAN_POINT('Ctrl Pts',(-20.3985411449705,24.2231919124203,-53.5158488246908));
#16394=CARTESIAN_POINT('Ctrl Pts',(-20.3993388247125,24.2269170621973,-53.5156136958505));
#16395=CARTESIAN_POINT('Ctrl Pts',(-20.4016851109997,24.2377800631558,-53.5149288502816));
#16396=CARTESIAN_POINT('Ctrl Pts',(-20.4032513922171,24.2449141325495,-53.514480123853));
#16397=CARTESIAN_POINT('Ctrl Pts',(-20.4086958305296,24.269315997934,-53.5129486150132));
#16398=CARTESIAN_POINT('Ctrl Pts',(-20.4126920462991,24.2865575007053,-53.5118722478569));
#16399=CARTESIAN_POINT('Ctrl Pts',(-20.4249737830639,24.3376300935813,-53.5086985548476));
#16400=CARTESIAN_POINT('Ctrl Pts',(-20.4336661736083,24.3713617577029,-53.5066216683911));
#16401=CARTESIAN_POINT('Ctrl Pts',(-20.4636689408993,24.4804405289553,-53.4999486693077));
#16402=CARTESIAN_POINT('Ctrl Pts',(-20.487179472856,24.5551569957334,-53.4954448115822));
#16403=CARTESIAN_POINT('Ctrl Pts',(-20.6334131949401,24.96685062181,-53.4706361289332));
#16404=CARTESIAN_POINT('Ctrl Pts',(-20.8089694298932,25.2823248171282,-53.4513217656664));
#16405=CARTESIAN_POINT('Ctrl Pts',(-21.0456445942043,25.5784230467081,-53.428399033085));
#16406=CARTESIAN_POINT('Ctrl Pts',(-21.0585768309744,25.5942898921396,-53.4271552459239));
#16407=CARTESIAN_POINT('Ctrl Pts',(-21.0756623826746,25.6148494388306,-53.425522854127));
#16408=CARTESIAN_POINT('Ctrl Pts',(-21.0796796649199,25.6196549825639,-53.4251398034008));
#16409=CARTESIAN_POINT('Ctrl Pts',(-21.085888884203,25.6270387091446,-53.4245489178817));
#16410=CARTESIAN_POINT('Ctrl Pts',(-21.0880709310687,25.6296252205906,-53.4243414891867));
#16411=CARTESIAN_POINT('Ctrl Pts',(-21.0924166666606,25.634760051124,-53.4239288120978));
#16412=CARTESIAN_POINT('Ctrl Pts',(-21.0945802548203,25.6373084500786,-53.423723567992));
#16413=CARTESIAN_POINT('Ctrl Pts',(-21.0993741784553,25.642937235037,-53.4232692709236));
#16414=CARTESIAN_POINT('Ctrl Pts',(-21.1020063610934,25.6460160340674,-53.4230201418249));
#16415=CARTESIAN_POINT('Ctrl Pts',(-21.1095847778396,25.6548465603615,-53.4223037480969));
#16416=CARTESIAN_POINT('Ctrl Pts',(-21.1145455004807,25.6605857676378,-53.4218358830612));
#16417=CARTESIAN_POINT('Ctrl Pts',(-21.1473021876072,25.6982135898575,-53.4187534375171));
#16418=CARTESIAN_POINT('Ctrl Pts',(-21.175702351635,25.7295685323623,-53.4161136640281));
#16419=CARTESIAN_POINT('Ctrl Pts',(-21.2613019078646,25.8204138387044,-53.408247043888));
#16420=CARTESIAN_POINT('Ctrl Pts',(-21.3201748464876,25.8782729101019,-53.4029490762581));
#16421=CARTESIAN_POINT('Ctrl Pts',(-21.5091359729717,26.0502291560515,-53.3862780052529));
#16422=CARTESIAN_POINT('Ctrl Pts',(-21.6462265176142,26.1561522626448,-53.3746224107306));
#16423=CARTESIAN_POINT('Ctrl Pts',(-21.8829307188597,26.3103535255527,-53.3554996505573));
#16424=CARTESIAN_POINT('Ctrl Pts',(-21.9776883720614,26.3654164988903,-53.3480832981571));
#16425=CARTESIAN_POINT('Ctrl Pts',(-22.0750361378578,26.4155368376325,-53.3407994113682));
#16426=CARTESIAN_POINT('Origin',(-23.5502525316942,23.5502525316942,-77.3107734492734));
#16427=CARTESIAN_POINT('',(-22.0750360141197,26.4155367739249,-51.843225903739));
#16428=CARTESIAN_POINT('',(-22.0750360382923,26.4155367863703,-52.0916569661403));
#16429=CARTESIAN_POINT('',(-22.0750360153461,26.4155367745563,-77.3107734492734));
#16430=CARTESIAN_POINT('Ctrl Pts',(-22.0750360141197,26.4155367739249,-51.843225903739));
#16431=CARTESIAN_POINT('Ctrl Pts',(-21.9897252008207,26.3716137595686,-51.8491828204502));
#16432=CARTESIAN_POINT('Ctrl Pts',(-21.9064243545153,26.3239056399464,-51.8552739078288));
#16433=CARTESIAN_POINT('Ctrl Pts',(-21.6581627873809,26.1666051315619,-51.8743120026963));
#16434=CARTESIAN_POINT('Ctrl Pts',(-21.5010827181033,26.0454858121205,-51.8876515832146));
#16435=CARTESIAN_POINT('Ctrl Pts',(-21.3324303570035,25.8887197230501,-51.903238253001));
#16436=CARTESIAN_POINT('Ctrl Pts',(-21.3090694962334,25.8663403152383,-51.9054276913812));
#16437=CARTESIAN_POINT('Ctrl Pts',(-21.2593355203793,25.8172386467926,-51.9101504072627));
#16438=CARTESIAN_POINT('Ctrl Pts',(-21.2330840939308,25.7903992470983,-51.9126821562577));
#16439=CARTESIAN_POINT('Ctrl Pts',(-21.1700493475658,25.7236587703121,-51.9188478690153));
#16440=CARTESIAN_POINT('Ctrl Pts',(-21.1337922148937,25.6832742995709,-51.9224696713775));
#16441=CARTESIAN_POINT('Ctrl Pts',(-21.0594741343531,25.5961677222589,-51.9300262087061));
#16442=CARTESIAN_POINT('Ctrl Pts',(-21.0216670562994,25.5492529042601,-51.9339501625412));
#16443=CARTESIAN_POINT('Ctrl Pts',(-20.9685029937478,25.4793577874751,-51.9395559324807));
#16444=CARTESIAN_POINT('Ctrl Pts',(-20.9520926830516,25.4571985955911,-51.9412993492558));
#16445=CARTESIAN_POINT('Ctrl Pts',(-20.9333886366962,25.4312523656387,-51.9432992499837));
#16446=CARTESIAN_POINT('Ctrl Pts',(-20.9308164781452,25.4276687833987,-51.9435745612431));
#16447=CARTESIAN_POINT('Ctrl Pts',(-20.9269177495744,25.4222133877612,-51.9439922856942));
#16448=CARTESIAN_POINT('Ctrl Pts',(-20.9255858204508,25.4203454386633,-51.9441350691902));
#16449=CARTESIAN_POINT('Ctrl Pts',(-20.9231748030695,25.4169564846848,-51.9443936663633));
#16450=CARTESIAN_POINT('Ctrl Pts',(-20.9220950438886,25.4154359703113,-51.9445095265595));
#16451=CARTESIAN_POINT('Ctrl Pts',(-20.9199253686315,25.4123750138554,-51.9447424354619));
#16452=CARTESIAN_POINT('Ctrl Pts',(-20.9188354900929,25.4108345579781,-51.944859481547));
#16453=CARTESIAN_POINT('Ctrl Pts',(-20.9157254645338,25.4064305876901,-51.9451936259339));
#16454=CARTESIAN_POINT('Ctrl Pts',(-20.9137086263029,25.403564722984,-51.9454104950953));
#16455=CARTESIAN_POINT('Ctrl Pts',(-20.9050673861997,25.3912431349876,-51.9463404740839));
#16456=CARTESIAN_POINT('Ctrl Pts',(-20.898489040387,25.3817549889842,-51.9470504502894));
#16457=CARTESIAN_POINT('Ctrl Pts',(-20.7860458814144,25.2176989716584,-51.9592247010205));
#16458=CARTESIAN_POINT('Ctrl Pts',(-20.6937888496416,25.054198587208,-51.9698193448342));
#16459=CARTESIAN_POINT('Ctrl Pts',(-20.5470902481273,24.7313880586405,-51.9896829837105));
#16460=CARTESIAN_POINT('Ctrl Pts',(-20.4898754918806,24.5740469823723,-51.9989449943794));
#16461=CARTESIAN_POINT('Ctrl Pts',(-20.4174652679603,24.3134282391892,-52.0144101571945));
#16462=CARTESIAN_POINT('Ctrl Pts',(-20.3946115001361,24.212611894009,-52.0204176289292));
#16463=CARTESIAN_POINT('Ctrl Pts',(-20.3711876067405,24.0800130107133,-52.0284466491232));
#16464=CARTESIAN_POINT('Ctrl Pts',(-20.3661858877997,24.0490706005728,-52.0303289482654));
#16465=CARTESIAN_POINT('Ctrl Pts',(-20.3597386947076,24.0051260647856,-52.0330165033216));
#16466=CARTESIAN_POINT('Ctrl Pts',(-20.3579197375424,23.9921798998042,-52.0338100125468));
#16467=CARTESIAN_POINT('Ctrl Pts',(-20.3552686898538,23.9724404612225,-52.0350226973708));
#16468=CARTESIAN_POINT('Ctrl Pts',(-20.3543793705177,23.9656549077074,-52.0354400675312));
#16469=CARTESIAN_POINT('Ctrl Pts',(-20.3529617851044,23.9545646066039,-52.0361230559527));
#16470=CARTESIAN_POINT('Ctrl Pts',(-20.3524205803886,23.9502615104261,-52.0363882652948));
#16471=CARTESIAN_POINT('Ctrl Pts',(-20.3513944330748,23.9419674666286,-52.0368998481531));
#16472=CARTESIAN_POINT('Ctrl Pts',(-20.3509082687275,23.9379766760756,-52.0371461825928));
#16473=CARTESIAN_POINT('Ctrl Pts',(-20.3500388952779,23.9307272475163,-52.0375939885858));
#16474=CARTESIAN_POINT('Ctrl Pts',(-20.3496531920863,23.9274689089441,-52.0377953810238));
#16475=CARTESIAN_POINT('Ctrl Pts',(-20.348885817436,23.9209003785849,-52.0382016167838));
#16476=CARTESIAN_POINT('Ctrl Pts',(-20.3485043026032,23.9175901733081,-52.0384064647653));
#16477=CARTESIAN_POINT('Ctrl Pts',(-20.3474494219307,23.9083110246299,-52.0389810492121));
#16478=CARTESIAN_POINT('Ctrl Pts',(-20.3467876120111,23.9023408045063,-52.0393511502678));
#16479=CARTESIAN_POINT('Ctrl Pts',(-20.3441639192748,23.8780524339338,-52.0408585179082));
#16480=CARTESIAN_POINT('Ctrl Pts',(-20.3423424669538,23.8597197519963,-52.0420002074042));
#16481=CARTESIAN_POINT('Ctrl Pts',(-20.3047465426246,23.4452280871383,-52.0679056645925));
#16482=CARTESIAN_POINT('Ctrl Pts',(-20.342484646457,23.0459015224298,-52.0954040832944));
#16483=CARTESIAN_POINT('Ctrl Pts',(-20.4601889674045,22.6345309650722,-52.1238185283854));
#16484=CARTESIAN_POINT('Ctrl Pts',(-20.4689505687567,22.6054683581212,-52.1258229624494));
#16485=CARTESIAN_POINT('Ctrl Pts',(-20.4921373287184,22.5323130346386,-52.1308540328354));
#16486=CARTESIAN_POINT('Ctrl Pts',(-20.5071069139545,22.4883981877375,-52.1338608174364));
#16487=CARTESIAN_POINT('Ctrl Pts',(-20.5322463792029,22.4195536727348,-52.138537026662));
#16488=CARTESIAN_POINT('Ctrl Pts',(-20.5417888464796,22.3944033125974,-52.140237295623));
#16489=CARTESIAN_POINT('Ctrl Pts',(-20.5532514083243,22.3652963983011,-52.1421931967453));
#16490=CARTESIAN_POINT('Ctrl Pts',(-20.5548656844681,22.3612216626441,-52.1424667354106));
#16491=CARTESIAN_POINT('Ctrl Pts',(-20.5573354074835,22.3550245676376,-52.1428823207265));
#16492=CARTESIAN_POINT('Ctrl Pts',(-20.5581848023828,22.3528998260356,-52.1430247319413));
#16493=CARTESIAN_POINT('Ctrl Pts',(-20.5597304440604,22.349045354493,-52.1432829369131));
#16494=CARTESIAN_POINT('Ctrl Pts',(-20.5604259266889,22.3473153299918,-52.1433987764799));
#16495=CARTESIAN_POINT('Ctrl Pts',(-20.5618296211566,22.3438323542216,-52.1436318857657));
#16496=CARTESIAN_POINT('Ctrl Pts',(-20.5625378712267,22.3420794296466,-52.1437491524705));
#16497=CARTESIAN_POINT('Ctrl Pts',(-20.564569989419,22.3370626353142,-52.1440846146279));
#16498=CARTESIAN_POINT('Ctrl Pts',(-20.5658976714384,22.3338002982404,-52.1443025780325));
#16499=CARTESIAN_POINT('Ctrl Pts',(-20.5716570002939,22.3197148436768,-52.1452428963538));
#16500=CARTESIAN_POINT('Ctrl Pts',(-20.5761422682075,22.3089135401885,-52.1459620310379));
#16501=CARTESIAN_POINT('Ctrl Pts',(-20.654939354486,22.1220353305908,-52.1583743839588));
#16502=CARTESIAN_POINT('Ctrl Pts',(-20.7447228958645,21.9528578399593,-52.1691635097813));
#16503=CARTESIAN_POINT('Ctrl Pts',(-20.9394544635006,21.6535801689934,-52.1891557525925));
#16504=CARTESIAN_POINT('Ctrl Pts',(-21.0405191250805,21.5217386785778,-52.1983528940377));
#16505=CARTESIAN_POINT('Ctrl Pts',(-21.2384687196092,21.3010698415384,-52.2153168950063));
#16506=CARTESIAN_POINT('Ctrl Pts',(-21.3314759240079,21.209271686118,-52.2229525751332));
#16507=CARTESIAN_POINT('Ctrl Pts',(-21.4402111670143,21.1142651248949,-52.2316838032351));
#16508=CARTESIAN_POINT('Ctrl Pts',(-21.450694459463,21.1052238817975,-52.2325236274529));
#16509=CARTESIAN_POINT('Ctrl Pts',(-21.4666692723492,21.0916250111101,-52.2338005809751));
#16510=CARTESIAN_POINT('Ctrl Pts',(-21.4721183045839,21.0870175416003,-52.2342356631949));
#16511=CARTESIAN_POINT('Ctrl Pts',(-21.4809978343844,21.0795598247708,-52.2349438859574));
#16512=CARTESIAN_POINT('Ctrl Pts',(-21.4844190457172,21.0766985172679,-52.2352165738291));
#16513=CARTESIAN_POINT('Ctrl Pts',(-21.491006537872,21.0712123111909,-52.235741281866));
#16514=CARTESIAN_POINT('Ctrl Pts',(-21.4941719274317,21.0685863521945,-52.2359932581151));
#16515=CARTESIAN_POINT('Ctrl Pts',(-21.4998777746368,21.063871278455,-52.2364471914248));
#16516=CARTESIAN_POINT('Ctrl Pts',(-21.5024164243122,21.0617799764888,-52.2366490591153));
#16517=CARTESIAN_POINT('Ctrl Pts',(-21.507498903764,21.0576061496168,-52.2370530156704));
#16518=CARTESIAN_POINT('Ctrl Pts',(-21.5100427275968,21.0555236234488,-52.2372551041527));
#16519=CARTESIAN_POINT('Ctrl Pts',(-21.5162902270514,21.0504249936557,-52.2377511925007));
#16520=CARTESIAN_POINT('Ctrl Pts',(-21.5199974217612,21.0474132310497,-52.2380453675553));
#16521=CARTESIAN_POINT('Ctrl Pts',(-21.5343171886579,21.0358324573817,-52.2391809264116));
#16522=CARTESIAN_POINT('Ctrl Pts',(-21.5449773086083,21.0273227094656,-52.2400246922209));
#16523=CARTESIAN_POINT('Ctrl Pts',(-21.719412853081,20.8898784734723,-52.2538070117694));
#16524=CARTESIAN_POINT('Ctrl Pts',(-21.8952302253688,20.7770892030371,-52.2673982957861));
#16525=CARTESIAN_POINT('Ctrl Pts',(-22.3317136485808,20.5534462080759,-52.3002945542933));
#16526=CARTESIAN_POINT('Ctrl Pts',(-22.5985599684848,20.4583309506143,-52.3198244506153));
#16527=CARTESIAN_POINT('Ctrl Pts',(-22.8913962245674,20.3955213901073,-52.3387921392178));
#16528=CARTESIAN_POINT('Ctrl Pts',(-22.9084358211156,20.3920106866872,-52.339886846749));
#16529=CARTESIAN_POINT('Ctrl Pts',(-22.9292935334166,20.3878891100563,-52.34121518554));
#16530=CARTESIAN_POINT('Ctrl Pts',(-22.9330849734733,20.3871469859516,-52.3414561763064));
#16531=CARTESIAN_POINT('Ctrl Pts',(-22.9390141573438,20.385997493308,-52.3418323017199));
#16532=CARTESIAN_POINT('Ctrl Pts',(-22.9411509788286,20.3855854723347,-52.3419677027523));
#16533=CARTESIAN_POINT('Ctrl Pts',(-22.9449351718859,20.3848597806119,-52.342207221219));
#16534=CARTESIAN_POINT('Ctrl Pts',(-22.946582361976,20.3845452330153,-52.3423113887773));
#16535=CARTESIAN_POINT('Ctrl Pts',(-22.9501091314918,20.3838746134338,-52.3425342267347));
#16536=CARTESIAN_POINT('Ctrl Pts',(-22.9519887773019,20.3835189302869,-52.3426528743032));
#16537=CARTESIAN_POINT('Ctrl Pts',(-22.9574394497188,20.3824925322029,-52.342996596076));
#16538=CARTESIAN_POINT('Ctrl Pts',(-22.9610113100484,20.3818261797711,-52.3432214196375));
#16539=CARTESIAN_POINT('Ctrl Pts',(-22.9770459874685,20.3788628651033,-52.3442288390815));
#16540=CARTESIAN_POINT('Ctrl Pts',(-22.9895213833982,20.3766333435147,-52.3450076217711));
#16541=CARTESIAN_POINT('Ctrl Pts',(-23.004438624141,20.3740581397258,-52.345933202787));
#16542=CARTESIAN_POINT('Ctrl Pts',(-23.0068678884837,20.3736416384814,-52.3460837548937));
#16543=CARTESIAN_POINT('Ctrl Pts',(-23.3467094626337,20.3157765020713,-52.3671205951503));
#16544=CARTESIAN_POINT('Ctrl Pts',(-23.6911834829049,20.3124289569336,-52.3852323126893));
#16545=CARTESIAN_POINT('Ctrl Pts',(-24.1691752316573,20.3843526014788,-52.4127896196593));
#16546=CARTESIAN_POINT('Ctrl Pts',(-24.307024525732,20.4144470088828,-52.4210040176603));
#16547=CARTESIAN_POINT('Ctrl Pts',(-24.4563526907502,20.4574690974191,-52.4303956750595));
#16548=CARTESIAN_POINT('Ctrl Pts',(-24.4702273715643,20.4615678354165,-52.4312729865578));
#16549=CARTESIAN_POINT('Ctrl Pts',(-24.4911277564164,20.467895366672,-52.4326018228255));
#16550=CARTESIAN_POINT('Ctrl Pts',(-24.4981743082336,20.470055105326,-52.433051093483));
#16551=CARTESIAN_POINT('Ctrl Pts',(-24.5095669990655,20.4735897139678,-52.4337795189083));
#16552=CARTESIAN_POINT('Ctrl Pts',(-24.5139177656754,20.4749496754266,-52.434058184442));
#16553=CARTESIAN_POINT('Ctrl Pts',(-24.5222525394739,20.4775743807511,-52.4345929639074));
#16554=CARTESIAN_POINT('Ctrl Pts',(-24.5262370027428,20.4788376547331,-52.4348490290793));
#16555=CARTESIAN_POINT('Ctrl Pts',(-24.5333604078968,20.4811113912041,-52.4353075634865));
#16556=CARTESIAN_POINT('Ctrl Pts',(-24.5365002833747,20.4821189282351,-52.435509936033));
#16557=CARTESIAN_POINT('Ctrl Pts',(-24.5427366890625,20.4841306559697,-52.4359124034262));
#16558=CARTESIAN_POINT('Ctrl Pts',(-24.5458332555072,20.4851347229186,-52.4361124939945));
#16559=CARTESIAN_POINT('Ctrl Pts',(-24.554275001186,20.4878861154398,-52.4366586673345));
#16560=CARTESIAN_POINT('Ctrl Pts',(-24.5596171181777,20.4896427366438,-52.4370050569881));
#16561=CARTESIAN_POINT('Ctrl Pts',(-24.5798305218702,20.4963480849113,-52.4383186182582));
#16562=CARTESIAN_POINT('Ctrl Pts',(-24.5946700478352,20.5013912285266,-52.4392889116558));
#16563=CARTESIAN_POINT('Ctrl Pts',(-24.8402609170771,20.5868575217609,-52.4554477012355));
#16564=CARTESIAN_POINT('Ctrl Pts',(-25.0611159308266,20.6931428451765,-52.4715512658913));
#16565=CARTESIAN_POINT('Ctrl Pts',(-25.3406135075725,20.8691837669334,-52.4938488210193));
#16566=CARTESIAN_POINT('Ctrl Pts',(-25.4115582344226,20.9179411652825,-52.4996864150406));
#16567=CARTESIAN_POINT('Ctrl Pts',(-25.5578974997907,21.0273913277006,-52.5120268035928));
#16568=CARTESIAN_POINT('Ctrl Pts',(-25.6326877518089,21.0887625961928,-52.5185168119012));
#16569=CARTESIAN_POINT('Ctrl Pts',(-25.7433796948718,21.1882558328908,-52.528291164311));
#16570=CARTESIAN_POINT('Ctrl Pts',(-25.7813018413411,21.2240421328298,-52.5316725871852));
#16571=CARTESIAN_POINT('Ctrl Pts',(-25.8360688989308,21.2782965947794,-52.5365841110802));
#16572=CARTESIAN_POINT('Ctrl Pts',(-25.8535926224181,21.2960642600643,-52.5381600798178));
#16573=CARTESIAN_POINT('Ctrl Pts',(-25.8738898504716,21.317127897949,-52.5399887744974));
#16574=CARTESIAN_POINT('Ctrl Pts',(-25.8768646884681,21.3202274440512,-52.5402568790687));
#16575=CARTESIAN_POINT('Ctrl Pts',(-25.8814018233075,21.3249737412854,-52.5406658999291));
#16576=CARTESIAN_POINT('Ctrl Pts',(-25.8829685783858,21.3266161944267,-52.5408071634393));
#16577=CARTESIAN_POINT('Ctrl Pts',(-25.8858065491106,21.3295975826021,-52.5410630798228));
#16578=CARTESIAN_POINT('Ctrl Pts',(-25.887078344656,21.3309359496986,-52.5411777780651));
#16579=CARTESIAN_POINT('Ctrl Pts',(-25.8896545006017,21.3336516229519,-52.5414101378102));
#16580=CARTESIAN_POINT('Ctrl Pts',(-25.8909587899795,21.3350289824253,-52.5415277938618));
#16581=CARTESIAN_POINT('Ctrl Pts',(-25.8947029085371,21.3389898561432,-52.5418655826252));
#16582=CARTESIAN_POINT('Ctrl Pts',(-25.8971396916499,21.3415762655819,-52.542085478115));
#16583=CARTESIAN_POINT('Ctrl Pts',(-25.9077619801233,21.3528882241219,-52.5430442924238));
#16584=CARTESIAN_POINT('Ctrl Pts',(-25.9159032763121,21.3616554320201,-52.5437798329132));
#16585=CARTESIAN_POINT('Ctrl Pts',(-25.9265323813206,21.3732303213727,-52.5447413505369));
#16586=CARTESIAN_POINT('Ctrl Pts',(-25.9290642424426,21.3759971480993,-52.5449704759604));
#16587=CARTESIAN_POINT('Ctrl Pts',(-25.9371213820002,21.3848329385137,-52.5456999370996));
#16588=CARTESIAN_POINT('Ctrl Pts',(-25.9426283600538,21.3909186477939,-52.5461989916147));
#16589=CARTESIAN_POINT('Ctrl Pts',(-25.9515706219715,21.4008768579321,-52.5470102665101));
#16590=CARTESIAN_POINT('Ctrl Pts',(-25.9550198898244,21.4047366702608,-52.5473234190469));
#16591=CARTESIAN_POINT('Ctrl Pts',(-25.9613889897607,21.4118984985006,-52.547902107237));
#16592=CARTESIAN_POINT('Ctrl Pts',(-25.9643113698717,21.4151982192778,-52.5481678074542));
#16593=CARTESIAN_POINT('Ctrl Pts',(-26.0355839570571,21.4960070087032,-52.5546524745252));
#16594=CARTESIAN_POINT('Ctrl Pts',(-26.1001804532907,21.5767610259256,-52.5606348081874));
#16595=CARTESIAN_POINT('Ctrl Pts',(-26.2810209898571,21.8265756214034,-52.5781747548292));
#16596=CARTESIAN_POINT('Ctrl Pts',(-26.3851290912829,22.0037603645225,-52.5894133206819));
#16597=CARTESIAN_POINT('Ctrl Pts',(-26.5233280854828,22.3004950621366,-52.6079906424235));
#16598=CARTESIAN_POINT('Ctrl Pts',(-26.568600824916,22.4141886879526,-52.615049940181));
#16599=CARTESIAN_POINT('Ctrl Pts',(-26.6239180850956,22.5799673676885,-52.6254463198742));
#16600=CARTESIAN_POINT('Ctrl Pts',(-26.6393139676713,22.6301589556454,-52.6286061686907));
#16601=CARTESIAN_POINT('Ctrl Pts',(-26.6556426107262,22.6884320949309,-52.632296163076));
#16602=CARTESIAN_POINT('Ctrl Pts',(-26.6577797374093,22.6961701749653,-52.6327865827214));
#16603=CARTESIAN_POINT('Ctrl Pts',(-26.6609761394213,22.7079144937432,-52.6335315799711));
#16604=CARTESIAN_POINT('Ctrl Pts',(-26.6620566474656,22.7119149632512,-52.6337854665638));
#16605=CARTESIAN_POINT('Ctrl Pts',(-26.6639136260692,22.7188432900237,-52.6342253755492));
#16606=CARTESIAN_POINT('Ctrl Pts',(-26.6646936917746,22.7217701854394,-52.6344112808681));
#16607=CARTESIAN_POINT('Ctrl Pts',(-26.666302875774,22.7278424172967,-52.6347971010998));
#16608=CARTESIAN_POINT('Ctrl Pts',(-26.6671313605615,22.7309879168528,-52.6349970363486));
#16609=CARTESIAN_POINT('Ctrl Pts',(-26.6691329088773,22.7386341557921,-52.6354832339393));
#16610=CARTESIAN_POINT('Ctrl Pts',(-26.670300991603,22.7431361815018,-52.635769657539));
#16611=CARTESIAN_POINT('Ctrl Pts',(-26.6746483965197,22.7600424233867,-52.6368458449617));
#16612=CARTESIAN_POINT('Ctrl Pts',(-26.6777634924159,22.7724628953724,-52.6376376859972));
#16613=CARTESIAN_POINT('Ctrl Pts',(-26.6820125117775,22.7898428615067,-52.6387474629635));
#16614=CARTESIAN_POINT('Ctrl Pts',(-26.6832088687879,22.794787093205,-52.6390633686789));
#16615=CARTESIAN_POINT('Ctrl Pts',(-26.7435070126344,23.0465902189239,-52.6551622434036));
#16616=CARTESIAN_POINT('Ctrl Pts',(-26.7732364955529,23.2995110305656,-52.6719416546303));
#16617=CARTESIAN_POINT('Ctrl Pts',(-26.7727822134999,23.7892719664017,-52.7050399444865));
#16618=CARTESIAN_POINT('Ctrl Pts',(-26.74663450226,24.0245852864968,-52.7211813837668));
#16619=CARTESIAN_POINT('Ctrl Pts',(-26.6919093968488,24.2688005347316,-52.7369922797257));
#16620=CARTESIAN_POINT('Ctrl Pts',(-26.6887136790122,24.2826327168205,-52.7378843248589));
#16621=CARTESIAN_POINT('Ctrl Pts',(-26.6845586641546,24.3000903021691,-52.7390053841722));
#16622=CARTESIAN_POINT('Ctrl Pts',(-26.683684366639,24.3037354778215,-52.7392391987727));
#16623=CARTESIAN_POINT('Ctrl Pts',(-26.682293171774,24.3094914360061,-52.7396079791744));
#16624=CARTESIAN_POINT('Ctrl Pts',(-26.6817804994965,24.3116032208455,-52.7397431888697));
#16625=CARTESIAN_POINT('Ctrl Pts',(-26.6808239338823,24.3155261661609,-52.7399941892723));
#16626=CARTESIAN_POINT('Ctrl Pts',(-26.6803806073414,24.3173374486916,-52.7401100118485));
#16627=CARTESIAN_POINT('Ctrl Pts',(-26.6793890147075,24.3213735881331,-52.740367951959));
#16628=CARTESIAN_POINT('Ctrl Pts',(-26.6788399490423,24.3235982403509,-52.7405100220968));
#16629=CARTESIAN_POINT('Ctrl Pts',(-26.6772301332399,24.3300909659134,-52.7409243656499));
#16630=CARTESIAN_POINT('Ctrl Pts',(-26.6761630132093,24.3343574775739,-52.7411962698606));
#16631=CARTESIAN_POINT('Ctrl Pts',(-26.6684199153631,24.3650485516147,-52.7431496318241));
#16632=CARTESIAN_POINT('Ctrl Pts',(-26.6614174397935,24.3913907012138,-52.7448124498148));
#16633=CARTESIAN_POINT('Ctrl Pts',(-26.6388375686339,24.4721895422076,-52.7498792864588));
#16634=CARTESIAN_POINT('Ctrl Pts',(-26.6221574882358,24.5263294480732,-52.7532272538077));
#16635=CARTESIAN_POINT('Ctrl Pts',(-26.5778971550926,24.6575866811807,-52.7612912292267));
#16636=CARTESIAN_POINT('Ctrl Pts',(-26.5487879202287,24.7341477377164,-52.7659496831208));
#16637=CARTESIAN_POINT('Ctrl Pts',(-26.4203244777721,25.0367774568539,-52.7844771973311));
#16638=CARTESIAN_POINT('Ctrl Pts',(-26.2980688754052,25.2521843940533,-52.7979958125178));
#16639=CARTESIAN_POINT('Ctrl Pts',(-26.0940359823415,25.5314334466337,-52.8181259133921));
#16640=CARTESIAN_POINT('Ctrl Pts',(-26.0320054169531,25.6086042117381,-52.824001394933));
#16641=CARTESIAN_POINT('Ctrl Pts',(-25.9603386306574,25.6898062313496,-52.8305936149293));
#16642=CARTESIAN_POINT('Ctrl Pts',(-25.9541192729382,25.6967915426531,-52.8311641608503));
#16643=CARTESIAN_POINT('Ctrl Pts',(-25.9448450461753,25.707117094005,-52.8320127249706));
#16644=CARTESIAN_POINT('Ctrl Pts',(-25.9418133662995,25.7104781737517,-52.832289764867));
#16645=CARTESIAN_POINT('Ctrl Pts',(-25.9366137460603,25.7162183849091,-52.8327643229604));
#16646=CARTESIAN_POINT('Ctrl Pts',(-25.9344492975762,25.7186006827458,-52.832961693014));
#16647=CARTESIAN_POINT('Ctrl Pts',(-25.9302334437901,25.7232269135209,-52.8333457884105));
#16648=CARTESIAN_POINT('Ctrl Pts',(-25.9281824246106,25.7254711943335,-52.8335324972004));
#16649=CARTESIAN_POINT('Ctrl Pts',(-25.9232722971412,25.730828745057,-52.8339791110253));
#16650=CARTESIAN_POINT('Ctrl Pts',(-25.9204102392042,25.7339392928263,-52.8342391417716));
#16651=CARTESIAN_POINT('Ctrl Pts',(-25.9118216983415,25.7432367322777,-52.8350185732211));
#16652=CARTESIAN_POINT('Ctrl Pts',(-25.9060770835053,25.749406758161,-52.8355387504125));
#16653=CARTESIAN_POINT('Ctrl Pts',(-25.8560379506446,25.802730419903,-52.8400599341334));
#16654=CARTESIAN_POINT('Ctrl Pts',(-25.810359853961,25.848559940563,-52.8441207453385));
#16655=CARTESIAN_POINT('Ctrl Pts',(-25.6899823962897,25.9622757817891,-52.8546693480358));
#16656=CARTESIAN_POINT('Ctrl Pts',(-25.6134213600829,26.0280804279194,-52.861238668793));
#16657=CARTESIAN_POINT('Ctrl Pts',(-25.2896809243261,26.2809178303072,-52.888431222496));
#16658=CARTESIAN_POINT('Ctrl Pts',(-25.019249989169,26.4354167404577,-52.9100221084945));
#16659=CARTESIAN_POINT('Ctrl Pts',(-24.69552290466,26.5628796624709,-52.9324049799868));
#16660=CARTESIAN_POINT('Ctrl Pts',(-24.6598587996901,26.5761971287406,-52.9348243576296));
#16661=CARTESIAN_POINT('Ctrl Pts',(-24.6190132081441,26.5906301008791,-52.9375359729122));
#16662=CARTESIAN_POINT('Ctrl Pts',(-24.614056888669,26.5923678217086,-52.9378640226648));
#16663=CARTESIAN_POINT('Ctrl Pts',(-24.6067946138255,26.5948941083061,-52.9383432348989));
#16664=CARTESIAN_POINT('Ctrl Pts',(-24.6044920093364,26.5956921756903,-52.9384949605713));
#16665=CARTESIAN_POINT('Ctrl Pts',(-24.6004485678798,26.5970884702414,-52.9387610149692));
#16666=CARTESIAN_POINT('Ctrl Pts',(-24.5987081226389,26.5976878180832,-52.938875410883));
#16667=CARTESIAN_POINT('Ctrl Pts',(-24.5953662701468,26.5988354321995,-52.9390948258316));
#16668=CARTESIAN_POINT('Ctrl Pts',(-24.5937649498605,26.5993839261605,-52.9391998584972));
#16669=CARTESIAN_POINT('Ctrl Pts',(-24.5894255088029,26.6008664790641,-52.9394842063217));
#16670=CARTESIAN_POINT('Ctrl Pts',(-24.5866865528256,26.6017981158596,-52.9396633764742));
#16671=CARTESIAN_POINT('Ctrl Pts',(-24.5807859339015,26.6037963095,-52.9400487222074));
#16672=CARTESIAN_POINT('Ctrl Pts',(-24.5776238575623,26.6048616482691,-52.9402548257505));
#16673=CARTESIAN_POINT('Ctrl Pts',(-24.5686967103348,26.6078538736223,-52.9408355854298));
#16674=CARTESIAN_POINT('Ctrl Pts',(-24.5629277967717,26.6097693759137,-52.9412095798552));
#16675=CARTESIAN_POINT('Ctrl Pts',(-24.5095554692257,26.6273235550072,-52.9446579174098));
#16676=CARTESIAN_POINT('Ctrl Pts',(-24.4615956852071,26.6418674058924,-52.9476702658952));
#16677=CARTESIAN_POINT('Ctrl Pts',(-24.34749374696,26.673582629561,-52.9546772186839));
#16678=CARTESIAN_POINT('Ctrl Pts',(-24.2811051910118,26.689781154413,-52.9586294484704));
#16679=CARTESIAN_POINT('Ctrl Pts',(-23.9179239977347,26.766249415111,-52.9798198191819));
#16680=CARTESIAN_POINT('Ctrl Pts',(-23.6142943556134,26.7865666865369,-52.9961470270256));
#16681=CARTESIAN_POINT('Ctrl Pts',(-23.2917089427677,26.7626812451586,-53.015092963649));
#16682=CARTESIAN_POINT('Ctrl Pts',(-23.2711539022192,26.7609607020362,-53.0163063600326));
#16683=CARTESIAN_POINT('Ctrl Pts',(-23.2460652795179,26.758617937616,-53.0177955641159));
#16684=CARTESIAN_POINT('Ctrl Pts',(-23.241514377516,26.7581832064688,-53.0180660245462));
#16685=CARTESIAN_POINT('Ctrl Pts',(-23.2329748418544,26.7573491156327,-53.0185741577171));
#16686=CARTESIAN_POINT('Ctrl Pts',(-23.2289859949089,26.7569519942754,-53.0188117657936));
#16687=CARTESIAN_POINT('Ctrl Pts',(-23.2199298932889,26.7560333205475,-53.0193518130592));
#16688=CARTESIAN_POINT('Ctrl Pts',(-23.2148631215906,26.7555071947111,-53.0196543839007));
#16689=CARTESIAN_POINT('Ctrl Pts',(-23.2029210869348,26.7542385258322,-53.0203685330292));
#16690=CARTESIAN_POINT('Ctrl Pts',(-23.196046942846,26.7534858642672,-53.0207804057505));
#16691=CARTESIAN_POINT('Ctrl Pts',(-23.1869868902137,26.7524643432857,-53.0213243143218));
#16692=CARTESIAN_POINT('Ctrl Pts',(-23.1847987250813,26.7522153559277,-53.0214557599027));
#16693=CARTESIAN_POINT('Ctrl Pts',(-23.1792324194128,26.7515761958789,-53.0217903440265));
#16694=CARTESIAN_POINT('Ctrl Pts',(-23.1758546436461,26.7511829195473,-53.0219935748054));
#16695=CARTESIAN_POINT('Ctrl Pts',(-23.1680403826476,26.7502605626194,-53.0224641953275));
#16696=CARTESIAN_POINT('Ctrl Pts',(-23.1636043697171,26.7497276016717,-53.0227317008958));
#16697=CARTESIAN_POINT('Ctrl Pts',(-23.1564103719225,26.7488481051033,-53.0231660850039));
#16698=CARTESIAN_POINT('Ctrl Pts',(-23.1536516920034,26.7485072218229,-53.0233327925871));
#16699=CARTESIAN_POINT('Ctrl Pts',(-23.1474122392505,26.7477280310845,-53.0237101504599));
#16700=CARTESIAN_POINT('Ctrl Pts',(-23.1439317380882,26.7472876085983,-53.0239208646709));
#16701=CARTESIAN_POINT('Ctrl Pts',(-23.1242116078043,26.7447595011469,-53.0251159826346));
#16702=CARTESIAN_POINT('Ctrl Pts',(-23.1079875783151,26.7425537929584,-53.0261039719001));
#16703=CARTESIAN_POINT('Ctrl Pts',(-23.0744713123119,26.7377367462865,-53.0281552212888));
#16704=CARTESIAN_POINT('Ctrl Pts',(-23.0571821488674,26.7351080960442,-53.0292189904562));
#16705=CARTESIAN_POINT('Ctrl Pts',(-23.034107913164,26.7314074934679,-53.0306465249964));
#16706=CARTESIAN_POINT('Ctrl Pts',(-23.0283029206094,26.7304601917093,-53.0310063253753));
#16707=CARTESIAN_POINT('Ctrl Pts',(-23.0192382585625,26.7289554653242,-53.031569210516));
#16708=CARTESIAN_POINT('Ctrl Pts',(-23.0159767781711,26.7284089025488,-53.0317719493782));
#16709=CARTESIAN_POINT('Ctrl Pts',(-23.0097414480619,26.727354109087,-53.0321599550066));
#16710=CARTESIAN_POINT('Ctrl Pts',(-23.0067674577324,26.7268467202684,-53.032345194781));
#16711=CARTESIAN_POINT('Ctrl Pts',(-22.9998185662771,26.725651134343,-53.0327784343979));
#16712=CARTESIAN_POINT('Ctrl Pts',(-22.99584424259,26.7249596496387,-53.0330265387658));
#16713=CARTESIAN_POINT('Ctrl Pts',(-22.9844755267049,26.7229596301403,-53.0337371699526));
#16714=CARTESIAN_POINT('Ctrl Pts',(-22.9770844321998,26.7216327170548,-53.0342002822185));
#16715=CARTESIAN_POINT('Ctrl Pts',(-22.9295702876154,26.7129310424172,-53.0371846699022));
#16716=CARTESIAN_POINT('Ctrl Pts',(-22.8895872167871,26.7048211084089,-53.039729335786));
#16717=CARTESIAN_POINT('Ctrl Pts',(-22.7711597115455,26.6784497737593,-53.0473701171001));
#16718=CARTESIAN_POINT('Ctrl Pts',(-22.6932390357195,26.6580056834719,-53.0525346651878));
#16719=CARTESIAN_POINT('Ctrl Pts',(-22.4835656934744,26.5945083613321,-53.0668102736648));
#16720=CARTESIAN_POINT('Ctrl Pts',(-22.3537003618806,26.5458444137825,-53.0760748887443));
#16721=CARTESIAN_POINT('Ctrl Pts',(-22.1759395151745,26.4658251380173,-53.0892395700871));
#16722=CARTESIAN_POINT('Ctrl Pts',(-22.1251412228718,26.4413338835681,-53.0930588162959));
#16723=CARTESIAN_POINT('Ctrl Pts',(-22.0750356956303,26.4155366099478,-53.096872577003));
#16724=CARTESIAN_POINT('',(-26.7730023713196,23.5492358241565,-52.9330225417352));
#16725=CARTESIAN_POINT('Ctrl Pts',(-22.0750361378578,26.4155368376325,-53.3407994113682));
#16726=CARTESIAN_POINT('Ctrl Pts',(-22.1242070858027,26.4408529252398,-53.3371202758974));
#16727=CARTESIAN_POINT('Ctrl Pts',(-22.1740388844405,26.464908014212,-53.3334755148323));
#16728=CARTESIAN_POINT('Ctrl Pts',(-22.2269649338975,26.4887955223206,-53.3297087672942));
#16729=CARTESIAN_POINT('Ctrl Pts',(-22.2294477788198,26.4899123383936,-53.3295323012437));
#16730=CARTESIAN_POINT('Ctrl Pts',(-22.2374274696282,26.4934895570924,-53.3289659225118));
#16731=CARTESIAN_POINT('Ctrl Pts',(-22.2429298310086,26.4959377132127,-53.3285765521788));
#16732=CARTESIAN_POINT('Ctrl Pts',(-22.2495689062746,26.4988693590425,-53.3281081830454));
#16733=CARTESIAN_POINT('Ctrl Pts',(-22.2506990376996,26.4993676200236,-53.3280285054649));
#16734=CARTESIAN_POINT('Ctrl Pts',(-22.2547703118536,26.5011597998254,-53.3277416501217));
#16735=CARTESIAN_POINT('Ctrl Pts',(-22.2577131132655,26.5024499741108,-53.3275346459821));
#16736=CARTESIAN_POINT('Ctrl Pts',(-22.2960583569796,26.5191928565472,-53.324841824636));
#16737=CARTESIAN_POINT('Ctrl Pts',(-22.3317359128781,26.5340131222827,-53.3223860159912));
#16738=CARTESIAN_POINT('Ctrl Pts',(-22.3720906754402,26.5499316400582,-53.319670548502));
#16739=CARTESIAN_POINT('Ctrl Pts',(-22.3765119975757,26.5516644114502,-53.3193738706306));
#16740=CARTESIAN_POINT('Ctrl Pts',(-22.3831776725568,26.5542597914343,-53.3189278635047));
#16741=CARTESIAN_POINT('Ctrl Pts',(-22.3854191626208,26.5551296615928,-53.318778099137));
#16742=CARTESIAN_POINT('Ctrl Pts',(-22.389303823817,26.5566322083863,-53.3185189235752));
#16743=CARTESIAN_POINT('Ctrl Pts',(-22.3909465396524,26.5572660467286,-53.3184094419626));
#16744=CARTESIAN_POINT('Ctrl Pts',(-22.3943355745528,26.5585705085772,-53.3181838154982));
#16745=CARTESIAN_POINT('Ctrl Pts',(-22.3960819561306,26.559240957123,-53.318067681718));
#16746=CARTESIAN_POINT('Ctrl Pts',(-22.4002116447766,26.5608222503166,-53.3177933694879));
#16747=CARTESIAN_POINT('Ctrl Pts',(-22.4025954583799,26.5617317885459,-53.3176352703644));
#16748=CARTESIAN_POINT('Ctrl Pts',(-22.4076482830864,26.5636528104836,-53.3173006696624));
#16749=CARTESIAN_POINT('Ctrl Pts',(-22.4103175652123,26.5646635822123,-53.317124210916));
#16750=CARTESIAN_POINT('Ctrl Pts',(-22.4175498291405,26.567391228943,-53.3166469160213));
#16751=CARTESIAN_POINT('Ctrl Pts',(-22.4221153923649,26.5691013067079,-53.3163464825931));
#16752=CARTESIAN_POINT('Ctrl Pts',(-22.4362753156447,26.5743684401869,-53.3154173476292));
#16753=CARTESIAN_POINT('Ctrl Pts',(-22.4458828614296,26.5778902087829,-53.314790688127));
#16754=CARTESIAN_POINT('Ctrl Pts',(-22.4818280557026,26.5908725113348,-53.3124595819443));
#16755=CARTESIAN_POINT('Ctrl Pts',(-22.5082726501679,26.6000359282977,-53.3107714852664));
#16756=CARTESIAN_POINT('Ctrl Pts',(-22.6011748115082,26.6308783095655,-53.304923630949));
#16757=CARTESIAN_POINT('Ctrl Pts',(-22.6682190529776,26.6507399100851,-53.3008499144153));
#16758=CARTESIAN_POINT('Ctrl Pts',(-23.1101907949546,26.7661730325682,-53.2746286820481));
#16759=CARTESIAN_POINT('Ctrl Pts',(-23.4990452924153,26.795743552224,-53.2540617875092));
#16760=CARTESIAN_POINT('Ctrl Pts',(-23.9038468104618,26.7536087247358,-53.229444444889));
#16761=CARTESIAN_POINT('Ctrl Pts',(-23.9237750551854,26.7513462056807,-53.228225586384));
#16762=CARTESIAN_POINT('Ctrl Pts',(-23.9498476209171,26.7481393238497,-53.2266214039715));
#16763=CARTESIAN_POINT('Ctrl Pts',(-23.9560124609934,26.7473629535743,-53.2262413978698));
#16764=CARTESIAN_POINT('Ctrl Pts',(-23.9655212291931,26.7461375194105,-53.2256541786737));
#16765=CARTESIAN_POINT('Ctrl Pts',(-23.9688667855917,26.7457010216763,-53.2254473635598));
#16766=CARTESIAN_POINT('Ctrl Pts',(-23.9755265554121,26.7448214771981,-53.2250352532907));
#16767=CARTESIAN_POINT('Ctrl Pts',(-23.9788407772145,26.7443785245904,-53.2248299613558));
#16768=CARTESIAN_POINT('Ctrl Pts',(-23.9861844897953,26.7433853867354,-53.2243746124204));
#16769=CARTESIAN_POINT('Ctrl Pts',(-23.990213635683,26.7428327309644,-53.2241244774278));
#16770=CARTESIAN_POINT('Ctrl Pts',(-24.001830915099,26.7412168430719,-53.2234023699143));
#16771=CARTESIAN_POINT('Ctrl Pts',(-24.0094162783063,26.7401341791878,-53.2229297819433));
#16772=CARTESIAN_POINT('Ctrl Pts',(-24.0604083389325,26.7326703981274,-53.2197453780736));
#16773=CARTESIAN_POINT('Ctrl Pts',(-24.1036829007203,26.7254307855831,-53.2170064200448));
#16774=CARTESIAN_POINT('Ctrl Pts',(-24.2193387200879,26.7036460381612,-53.2095834433729));
#16775=CARTESIAN_POINT('Ctrl Pts',(-24.2913868661905,26.6874942228014,-53.2048498271766));
#16776=CARTESIAN_POINT('Ctrl Pts',(-24.5290458550738,26.6255721288829,-53.1888669227109));
#16777=CARTESIAN_POINT('Ctrl Pts',(-24.6915329526469,26.569042715956,-53.1773161269921));
#16778=CARTESIAN_POINT('Ctrl Pts',(-24.9204693055348,26.4682601441986,-53.16038715081));
#16779=CARTESIAN_POINT('Ctrl Pts',(-24.9910389467116,26.4340689702133,-53.155075776131));
#16780=CARTESIAN_POINT('Ctrl Pts',(-25.1866491189176,26.3303210743683,-53.1401860839456));
#16781=CARTESIAN_POINT('Ctrl Pts',(-25.3084224856917,26.2549566596191,-53.1307119714078));
#16782=CARTESIAN_POINT('Ctrl Pts',(-25.4309513998696,26.1673399481675,-53.1212567724125));
#16783=CARTESIAN_POINT('Ctrl Pts',(-25.4370888499931,26.1629185051618,-53.1207833954757));
#16784=CARTESIAN_POINT('Ctrl Pts',(-25.4453594817836,26.1569159659023,-53.1201458661596));
#16785=CARTESIAN_POINT('Ctrl Pts',(-25.4475062955394,26.1553538286141,-53.1199804168128));
#16786=CARTESIAN_POINT('Ctrl Pts',(-25.4511283610704,26.152711366567,-53.1197013355821));
#16787=CARTESIAN_POINT('Ctrl Pts',(-25.4526046233393,26.1516324396212,-53.1195876065431));
#16788=CARTESIAN_POINT('Ctrl Pts',(-25.4555517207012,26.1494747018895,-53.1193606027074));
#16789=CARTESIAN_POINT('Ctrl Pts',(-25.4570225479631,26.1483959062484,-53.1192473286528));
#16790=CARTESIAN_POINT('Ctrl Pts',(-25.4603755945292,26.1459321937484,-53.1189891381115));
#16791=CARTESIAN_POINT('Ctrl Pts',(-25.4622572211323,26.1445464801175,-53.118844278474));
#16792=CARTESIAN_POINT('Ctrl Pts',(-25.4676461819518,26.1405687618566,-53.118429479627));
#16793=CARTESIAN_POINT('Ctrl Pts',(-25.4711497814763,26.1379716699706,-53.118159895323));
#16794=CARTESIAN_POINT('Ctrl Pts',(-25.4792297236193,26.1319568483895,-53.1175383757674));
#16795=CARTESIAN_POINT('Ctrl Pts',(-25.4838022902211,26.1285340365482,-53.117186790272));
#16796=CARTESIAN_POINT('Ctrl Pts',(-25.4985003311128,26.1174706712513,-53.1160570276572));
#16797=CARTESIAN_POINT('Ctrl Pts',(-25.5085899529218,26.1097823753797,-53.1152820619451));
#16798=CARTESIAN_POINT('Ctrl Pts',(-25.5483460986055,26.0791154674509,-53.1122295721013));
#16799=CARTESIAN_POINT('Ctrl Pts',(-25.5776569681329,26.0556780785861,-53.1099815292837));
#16800=CARTESIAN_POINT('Ctrl Pts',(-25.6580960610054,25.9890215159716,-53.1037979655626));
#16801=CARTESIAN_POINT('Ctrl Pts',(-25.7082988726084,25.944711878643,-53.0999221874937));
#16802=CARTESIAN_POINT('Ctrl Pts',(-25.9753875224474,25.6937467315603,-53.0789802995716));
#16803=CARTESIAN_POINT('Ctrl Pts',(-26.1640207033375,25.4591988905828,-53.0628291597259));
#16804=CARTESIAN_POINT('Ctrl Pts',(-26.330634000495,25.1800524022947,-53.0438306872907));
#16805=CARTESIAN_POINT('Ctrl Pts',(-26.3434514159162,25.1579865501049,-53.0423314803646));
#16806=CARTESIAN_POINT('Ctrl Pts',(-26.3593321837937,25.1298837550343,-53.0404240642853));
#16807=CARTESIAN_POINT('Ctrl Pts',(-26.3626406094728,25.1239858612637,-53.0400238660999));
#16808=CARTESIAN_POINT('Ctrl Pts',(-26.3946250702387,25.0665445437146,-53.036127103292));
#16809=CARTESIAN_POINT('Ctrl Pts',(-26.4218980096098,25.0142361947054,-53.0325851575725));
#16810=CARTESIAN_POINT('Ctrl Pts',(-26.4516682062971,24.9531017779214,-53.0284422208177));
#16811=CARTESIAN_POINT('Ctrl Pts',(-26.4555832131071,24.9449756416725,-53.0278914716006));
#16812=CARTESIAN_POINT('Ctrl Pts',(-26.4613336150686,24.9329106133996,-53.0270736368709));
#16813=CARTESIAN_POINT('Ctrl Pts',(-26.4631952647835,24.928984223625,-53.0268074645185));
#16814=CARTESIAN_POINT('Ctrl Pts',(-26.4664864968954,24.9220062917865,-53.0263343863021));
#16815=CARTESIAN_POINT('Ctrl Pts',(-26.4679192476806,24.9189562441202,-53.02612759072));
#16816=CARTESIAN_POINT('Ctrl Pts',(-26.4709147322618,24.9125533634978,-53.0256934395702));
#16817=CARTESIAN_POINT('Ctrl Pts',(-26.4724764815431,24.9092000777404,-53.0254660502804));
#16818=CARTESIAN_POINT('Ctrl Pts',(-26.4765528259633,24.9004080978849,-53.0248698077752));
#16819=CARTESIAN_POINT('Ctrl Pts',(-26.4790580241223,24.8949650853286,-53.0245006303804));
#16820=CARTESIAN_POINT('Ctrl Pts',(-26.4900061995884,24.8710023935305,-53.0228750886804));
#16821=CARTESIAN_POINT('Ctrl Pts',(-26.49828865636,24.852410280394,-53.0216132085418));
#16822=CARTESIAN_POINT('Ctrl Pts',(-26.5558032136623,24.7199422841882,-53.0126162127485));
#16823=CARTESIAN_POINT('Ctrl Pts',(-26.5985937073975,24.6033994440204,-53.0046625705489));
#16824=CARTESIAN_POINT('Ctrl Pts',(-26.7264677726202,24.1813255691787,-52.9757115417625));
#16825=CARTESIAN_POINT('Ctrl Pts',(-26.7731023432559,23.8661259127418,-52.9536327572046));
#16826=CARTESIAN_POINT('Ctrl Pts',(-26.7730023713196,23.5492358241565,-52.9330225417352));
#16827=CARTESIAN_POINT('Ctrl Pts',(-26.7730023700881,23.5492319278606,-52.9330222883241));
#16828=CARTESIAN_POINT('Ctrl Pts',(-26.7729846809421,23.4933751003751,-52.9293894185385));
#16829=CARTESIAN_POINT('Ctrl Pts',(-26.7715148199125,23.4375231614134,-52.9258125164439));
#16830=CARTESIAN_POINT('Ctrl Pts',(-26.7683879685189,23.3778073947579,-52.9220675012335));
#16831=CARTESIAN_POINT('Ctrl Pts',(-26.7681752323791,23.3738821605883,-52.9218217019452));
#16832=CARTESIAN_POINT('Ctrl Pts',(-26.7678175169938,23.3674980660912,-52.9214225373896));
#16833=CARTESIAN_POINT('Ctrl Pts',(-26.7676769006209,23.3650389801996,-52.9212689304832));
#16834=CARTESIAN_POINT('Ctrl Pts',(-26.7674249622829,23.3607199857685,-52.9209994055313));
#16835=CARTESIAN_POINT('Ctrl Pts',(-26.7673148465426,23.3588600121708,-52.9208834198018));
#16836=CARTESIAN_POINT('Ctrl Pts',(-26.7670964996327,23.3552253291779,-52.9206569330345));
#16837=CARTESIAN_POINT('Ctrl Pts',(-26.7669884126037,23.3534506101768,-52.9205464237487));
#16838=CARTESIAN_POINT('Ctrl Pts',(-26.7667702857427,23.3499172998788,-52.9203265661706));
#16839=CARTESIAN_POINT('Ctrl Pts',(-26.7666602725296,23.348158712028,-52.9202172165389));
#16840=CARTESIAN_POINT('Ctrl Pts',(-26.7663964209443,23.3439957725703,-52.9199585442965));
#16841=CARTESIAN_POINT('Ctrl Pts',(-26.7662413283009,23.3415914973977,-52.9198092928672));
#16842=CARTESIAN_POINT('Ctrl Pts',(-26.7657712726286,23.3344296345318,-52.9193651217387));
#16843=CARTESIAN_POINT('Ctrl Pts',(-26.7654484456831,23.3296725425759,-52.9190706435319));
#16844=CARTESIAN_POINT('Ctrl Pts',(-26.7623754740257,23.285830614817,-52.9163616383671));
#16845=CARTESIAN_POINT('Ctrl Pts',(-26.7589231746487,23.2467961252311,-52.913985887441));
#16846=CARTESIAN_POINT('Ctrl Pts',(-26.7536069219483,23.1970444965563,-52.9109931063958));
#16847=CARTESIAN_POINT('Ctrl Pts',(-26.7523997120542,23.1862625495263,-52.9103466444932));
#16848=CARTESIAN_POINT('Ctrl Pts',(-26.7497714237146,23.1638142608957,-52.9090047330167));
#16849=CARTESIAN_POINT('Ctrl Pts',(-26.7483409286878,23.1521491659268,-52.9083096942081));
#16850=CARTESIAN_POINT('Ctrl Pts',(-26.7100243515173,22.8532366631737,-52.8905521352205));
#16851=CARTESIAN_POINT('Ctrl Pts',(-26.6346483054277,22.5722281342401,-52.8749936966126));
#16852=CARTESIAN_POINT('Ctrl Pts',(-26.4847514209994,22.2144035730923,-52.852896990685));
#16853=CARTESIAN_POINT('Ctrl Pts',(-26.4426550919353,22.1255486306699,-52.8472156412204));
#16854=CARTESIAN_POINT('Ctrl Pts',(-26.3666885058268,21.9824947123475,-52.8376316119333));
#16855=CARTESIAN_POINT('Ctrl Pts',(-26.3351493004389,21.9271304471426,-52.8338088275422));
#16856=CARTESIAN_POINT('Ctrl Pts',(-26.2976183388697,21.8655658312983,-52.8294137365891));
#16857=CARTESIAN_POINT('Ctrl Pts',(-26.2932168809969,21.8584089416198,-52.8289005585163));
#16858=CARTESIAN_POINT('Ctrl Pts',(-26.2865621144583,21.8476823424888,-52.8281280003493));
#16859=CARTESIAN_POINT('Ctrl Pts',(-26.2843296728532,21.8440996757573,-52.8278693916304));
#16860=CARTESIAN_POINT('Ctrl Pts',(-26.2804776170884,21.8379447950353,-52.8274241165647));
#16861=CARTESIAN_POINT('Ctrl Pts',(-26.2788613870028,21.8353704609487,-52.8272375758316));
#16862=CARTESIAN_POINT('Ctrl Pts',(-26.2755249184386,21.830072786325,-52.8268530758884));
#16863=CARTESIAN_POINT('Ctrl Pts',(-26.273804234564,21.8273497311863,-52.8266551002596));
#16864=CARTESIAN_POINT('Ctrl Pts',(-26.269651257089,21.8207992365135,-52.8261780368822));
#16865=CARTESIAN_POINT('Ctrl Pts',(-26.2672149663771,21.8169743497265,-52.8258988004754));
#16866=CARTESIAN_POINT('Ctrl Pts',(-26.2597108523121,21.8052478641991,-52.8250406224921));
#16867=CARTESIAN_POINT('Ctrl Pts',(-26.2546166061976,21.7973633080732,-52.8244606948665));
#16868=CARTESIAN_POINT('Ctrl Pts',(-26.1946266885844,21.7053986387906,-52.8176620423596));
#16869=CARTESIAN_POINT('Ctrl Pts',(-26.1358703017428,21.623914635597,-52.8112976776001));
#16870=CARTESIAN_POINT('Ctrl Pts',(-25.892740352064,21.3179426178945,-52.7859931730411));
#16871=CARTESIAN_POINT('Ctrl Pts',(-25.6821743014006,21.1160551253123,-52.7660086614789));
#16872=CARTESIAN_POINT('Ctrl Pts',(-25.3924477802677,20.9050549188075,-52.7420696772945));
#16873=CARTESIAN_POINT('Ctrl Pts',(-25.3361474461298,20.8667223461637,-52.7375688992182));
#16874=CARTESIAN_POINT('Ctrl Pts',(-25.2489454289872,20.8113110484331,-52.7308681905592));
#16875=CARTESIAN_POINT('Ctrl Pts',(-25.21891015265,20.7929096106098,-52.7286070161654));
#16876=CARTESIAN_POINT('Ctrl Pts',(-25.1781502289098,20.7688476205305,-52.7256068434281));
#16877=CARTESIAN_POINT('Ctrl Pts',(-25.1676877694296,20.7627505218464,-52.7248427025274));
#16878=CARTESIAN_POINT('Ctrl Pts',(-25.1524067934221,20.75396038914,-52.7237355597798));
#16879=CARTESIAN_POINT('Ctrl Pts',(-25.14761547994,20.7512206209232,-52.7233896873278));
#16880=CARTESIAN_POINT('Ctrl Pts',(-25.1390306106827,20.7463408447419,-52.722772268801));
#16881=CARTESIAN_POINT('Ctrl Pts',(-25.135239725249,20.7441962013078,-52.7225004302937));
#16882=CARTESIAN_POINT('Ctrl Pts',(-25.1294652392343,20.7409447973587,-52.7220875799382));
#16883=CARTESIAN_POINT('Ctrl Pts',(-25.127484816265,20.7398324487818,-52.7219462078476));
#16884=CARTESIAN_POINT('Ctrl Pts',(-25.123885008566,20.7378155402523,-52.7216896370563));
#16885=CARTESIAN_POINT('Ctrl Pts',(-25.1222660228562,20.7369102868263,-52.7215743934975));
#16886=CARTESIAN_POINT('Ctrl Pts',(-25.1187700654545,20.7349594874613,-52.7213258600931));
#16887=CARTESIAN_POINT('Ctrl Pts',(-25.1168928345929,20.7339144234376,-52.721192601792));
#16888=CARTESIAN_POINT('Ctrl Pts',(-25.1118300864111,20.7311025938544,-52.7208337416046));
#16889=CARTESIAN_POINT('Ctrl Pts',(-25.1086426043639,20.729339343889,-52.7206083669186));
#16890=CARTESIAN_POINT('Ctrl Pts',(-25.0939297892302,20.7212330630903,-52.7195706369741));
#16891=CARTESIAN_POINT('Ctrl Pts',(-25.0823684602513,20.7149551179017,-52.7187624141991));
#16892=CARTESIAN_POINT('Ctrl Pts',(-25.0607716447043,20.7033984553046,-52.7172654340763));
#16893=CARTESIAN_POINT('Ctrl Pts',(-25.0507461850442,20.6981016016644,-52.7165756095101));
#16894=CARTESIAN_POINT('Ctrl Pts',(-25.037349563696,20.6911138155179,-52.7156603071847));
#16895=CARTESIAN_POINT('Ctrl Pts',(-25.034003235573,20.6893758076924,-52.7154322112815));
#16896=CARTESIAN_POINT('Ctrl Pts',(-25.025463825841,20.6849596425712,-52.7148514861295));
#16897=CARTESIAN_POINT('Ctrl Pts',(-25.0202664723663,20.6822897149665,-52.7144993059205));
#16898=CARTESIAN_POINT('Ctrl Pts',(-24.8641076946396,20.6026055552911,-52.7039548752677));
#16899=CARTESIAN_POINT('Ctrl Pts',(-24.7072922915293,20.5375939392647,-52.694397323582));
#16900=CARTESIAN_POINT('Ctrl Pts',(-24.5297422393207,20.4799085240806,-52.6839457206577));
#16901=CARTESIAN_POINT('Ctrl Pts',(-24.5133691689411,20.4747332652562,-52.6829853581581));
#16902=CARTESIAN_POINT('Ctrl Pts',(-24.4783652700363,20.4639760466004,-52.6809382450173));
#16903=CARTESIAN_POINT('Ctrl Pts',(-24.4597237072971,20.4584313888354,-52.6798516649791));
#16904=CARTESIAN_POINT('Ctrl Pts',(-24.4195497668452,20.4468770162364,-52.6775159366981));
#16905=CARTESIAN_POINT('Ctrl Pts',(-24.3980027712868,20.4409219282711,-52.6762668211985));
#16906=CARTESIAN_POINT('Ctrl Pts',(-24.3510724440081,20.4284755703248,-52.6735513610455));
#16907=CARTESIAN_POINT('Ctrl Pts',(-24.3256684571303,20.422068704251,-52.6720847049147));
#16908=CARTESIAN_POINT('Ctrl Pts',(-24.269432814875,20.4086132461758,-52.6688410125533));
#16909=CARTESIAN_POINT('Ctrl Pts',(-24.2385699781465,20.4017073542298,-52.6670627851326));
#16910=CARTESIAN_POINT('Ctrl Pts',(-24.1682199773021,20.3870495986992,-52.6630067835336));
#16911=CARTESIAN_POINT('Ctrl Pts',(-24.128679635947,20.3795809106773,-52.6607252026832));
#16912=CARTESIAN_POINT('Ctrl Pts',(-23.953491649148,20.3498761232679,-52.6505825626587));
#16913=CARTESIAN_POINT('Ctrl Pts',(-23.8166574421841,20.3355935636925,-52.6425631548651));
#16914=CARTESIAN_POINT('Ctrl Pts',(-23.6577046317934,20.3292215688205,-52.6329474442502));
#16915=CARTESIAN_POINT('Ctrl Pts',(-23.6360611788002,20.3285723399105,-52.6316319483899));
#16916=CARTESIAN_POINT('Ctrl Pts',(-23.60828701155,20.3280192832981,-52.6299353808698));
#16917=CARTESIAN_POINT('Ctrl Pts',(-23.6021604923769,20.3279147668533,-52.6295606197009));
#16918=CARTESIAN_POINT('Ctrl Pts',(-23.59230462753,20.3277747438942,-52.6289568735553));
#16919=CARTESIAN_POINT('Ctrl Pts',(-23.5885754327827,20.3277282374964,-52.6287282342494));
#16920=CARTESIAN_POINT('Ctrl Pts',(-23.5814836559181,20.3276521085517,-52.6282930532253));
#16921=CARTESIAN_POINT('Ctrl Pts',(-23.5781210894881,20.3276212754521,-52.6280865498061));
#16922=CARTESIAN_POINT('Ctrl Pts',(-23.5704704793238,20.3275630981307,-52.6276163351458));
#16923=CARTESIAN_POINT('Ctrl Pts',(-23.5661824234213,20.3275390494135,-52.6273525207771));
#16924=CARTESIAN_POINT('Ctrl Pts',(-23.5531622804205,20.3274920153239,-52.6265506670712));
#16925=CARTESIAN_POINT('Ctrl Pts',(-23.5444301897244,20.327495961545,-52.6260117832615));
#16926=CARTESIAN_POINT('Ctrl Pts',(-23.4827716447314,20.327774420141,-52.6221986595597));
#16927=CARTESIAN_POINT('Ctrl Pts',(-23.4298616568506,20.3293172096997,-52.6188848050576));
#16928=CARTESIAN_POINT('Ctrl Pts',(-23.373197642625,20.3323675506224,-52.6152881311864));
#16929=CARTESIAN_POINT('Ctrl Pts',(-23.3693795959243,20.3325798997977,-52.6150455542441));
#16930=CARTESIAN_POINT('Ctrl Pts',(-23.3615276202858,20.3330306245585,-52.614546207307));
#16931=CARTESIAN_POINT('Ctrl Pts',(-23.3574937451056,20.3332697928693,-52.6142894136466));
#16932=CARTESIAN_POINT('Ctrl Pts',(-23.3487856836105,20.3338025311705,-52.6137345040127));
#16933=CARTESIAN_POINT('Ctrl Pts',(-23.3441116708571,20.3340987042363,-52.6134363099638));
#16934=CARTESIAN_POINT('Ctrl Pts',(-23.3203134292723,20.3356587928656,-52.6119162428206));
#16935=CARTESIAN_POINT('Ctrl Pts',(-23.3012004137643,20.3370830816991,-52.6106895777369));
#16936=CARTESIAN_POINT('Ctrl Pts',(-23.1338318425769,20.3510575486446,-52.599896404522));
#16937=CARTESIAN_POINT('Ctrl Pts',(-22.9866149287709,20.3736886757336,-52.5900354302345));
#16938=CARTESIAN_POINT('Ctrl Pts',(-22.6816982268951,20.4424291117452,-52.568999678416));
#16939=CARTESIAN_POINT('Ctrl Pts',(-22.5248741610673,20.4905871048004,-52.5578215368336));
#16940=CARTESIAN_POINT('Ctrl Pts',(-22.3064547977899,20.5763489307018,-52.5421689771781));
#16941=CARTESIAN_POINT('Ctrl Pts',(-22.241385379507,20.6044073945811,-52.5374971529268));
#16942=CARTESIAN_POINT('Ctrl Pts',(-22.1497762967372,20.6475453963387,-52.5309566993903));
#16943=CARTESIAN_POINT('Ctrl Pts',(-22.1224465759216,20.6608905425067,-52.5290103704465));
#16944=CARTESIAN_POINT('Ctrl Pts',(-22.0856048948449,20.6795308223162,-52.5263973462573));
#16945=CARTESIAN_POINT('Ctrl Pts',(-22.0759257880804,20.6844897198558,-52.525711865537));
#16946=CARTESIAN_POINT('Ctrl Pts',(-22.0617456582692,20.6918454842499,-52.5247093220912));
#16947=CARTESIAN_POINT('Ctrl Pts',(-22.057225048281,20.6942041259904,-52.5243899678195));
#16948=CARTESIAN_POINT('Ctrl Pts',(-22.049092654813,20.6984718116124,-52.5238159492891));
#16949=CARTESIAN_POINT('Ctrl Pts',(-22.0454788795865,20.7003770067366,-52.5235610475396));
#16950=CARTESIAN_POINT('Ctrl Pts',(-22.0399139815044,20.7033243768008,-52.5231688006567));
#16951=CARTESIAN_POINT('Ctrl Pts',(-22.0379603094413,20.70436168876,-52.5230311475306));
#16952=CARTESIAN_POINT('Ctrl Pts',(-22.0343946316353,20.7062596117828,-52.5227800140398));
#16953=CARTESIAN_POINT('Ctrl Pts',(-22.032782296213,20.7071195790957,-52.5226664933345));
#16954=CARTESIAN_POINT('Ctrl Pts',(-22.0294951409166,20.7088764336983,-52.5224351287521));
#16955=CARTESIAN_POINT('Ctrl Pts',(-22.027820389043,20.7097734272234,-52.5223172924593));
#16956=CARTESIAN_POINT('Ctrl Pts',(-22.0230029330546,20.7123591309059,-52.5219784469385));
#16957=CARTESIAN_POINT('Ctrl Pts',(-22.0198622259353,20.714051586219,-52.5217576772823));
#16958=CARTESIAN_POINT('Ctrl Pts',(-22.0060941810934,20.7215003993676,-52.5207904592404));
#16959=CARTESIAN_POINT('Ctrl Pts',(-21.9954962825397,20.7273113961944,-52.5200474622675));
#16960=CARTESIAN_POINT('Ctrl Pts',(-21.9818484038171,20.7348949182651,-52.5190922723478));
#16961=CARTESIAN_POINT('Ctrl Pts',(-21.9787684765839,20.7366129199762,-52.5188768219932));
#16962=CARTESIAN_POINT('Ctrl Pts',(-21.7362387455544,20.8724199010594,-52.501919152427));
#16963=CARTESIAN_POINT('Ctrl Pts',(-21.5148488996317,21.036565762169,-52.486992278037));
#16964=CARTESIAN_POINT('Ctrl Pts',(-21.29123604148,21.2515069399556,-52.4695907613846));
#16965=CARTESIAN_POINT('Ctrl Pts',(-21.2659627632611,21.2766195367824,-52.4675865999366));
#16966=CARTESIAN_POINT('Ctrl Pts',(-21.2111013842029,21.3329703602861,-52.4631424840714));
#16967=CARTESIAN_POINT('Ctrl Pts',(-21.1817123168005,21.3643921930242,-52.4606988605834));
#16968=CARTESIAN_POINT('Ctrl Pts',(-21.0656658257457,21.4935543317127,-52.45076266473));
#16969=CARTESIAN_POINT('Ctrl Pts',(-20.9843673515529,21.5959225675316,-52.4431245433296));
#16970=CARTESIAN_POINT('Ctrl Pts',(-20.9015721998513,21.7142781882836,-52.4343905157874));
#16971=CARTESIAN_POINT('Ctrl Pts',(-20.8937084773239,21.7256750551589,-52.4335505110737));
#16972=CARTESIAN_POINT('Ctrl Pts',(-20.8800766596713,21.7457065513532,-52.4320756934417));
#16973=CARTESIAN_POINT('Ctrl Pts',(-20.8742763586644,21.7543190974858,-52.4314421079183));
#16974=CARTESIAN_POINT('Ctrl Pts',(-20.8659648654255,21.7667900346747,-52.4305253580512));
#16975=CARTESIAN_POINT('Ctrl Pts',(-20.8634201177541,21.7706260729648,-52.4302434597304));
#16976=CARTESIAN_POINT('Ctrl Pts',(-20.859005162701,21.7773123795494,-52.4297522590103));
#16977=CARTESIAN_POINT('Ctrl Pts',(-20.8571312381472,21.7801601944703,-52.429543096743));
#16978=CARTESIAN_POINT('Ctrl Pts',(-20.8535277130482,21.7856554628002,-52.4291395794258));
#16979=CARTESIAN_POINT('Ctrl Pts',(-20.8517974828563,21.7883025005263,-52.4289452482965));
#16980=CARTESIAN_POINT('Ctrl Pts',(-20.8477168525667,21.7945654682021,-52.4284855491162));
#16981=CARTESIAN_POINT('Ctrl Pts',(-20.8453698131854,21.7981835716638,-52.4282200556442));
#16982=CARTESIAN_POINT('Ctrl Pts',(-20.8384190908077,21.808945785676,-52.4274305450019));
#16983=CARTESIAN_POINT('Ctrl Pts',(-20.8338364251998,21.8161033659659,-52.4269057449411));
#16984=CARTESIAN_POINT('Ctrl Pts',(-20.7922609554316,21.8816084910158,-52.4221052132072));
#16985=CARTESIAN_POINT('Ctrl Pts',(-20.7571274699602,21.9411093853614,-52.4177611520951));
#16986=CARTESIAN_POINT('Ctrl Pts',(-20.7187300584901,22.0111893810128,-52.4126575085473));
#16987=CARTESIAN_POINT('Ctrl Pts',(-20.7135730811969,22.0207151543435,-52.4119640662908));
#16988=CARTESIAN_POINT('Ctrl Pts',(-20.5858623426182,22.2594850554161,-52.3945894036664));
#16989=CARTESIAN_POINT('Ctrl Pts',(-20.4914607565009,22.5026651396318,-52.3769365680758));
#16990=CARTESIAN_POINT('Ctrl Pts',(-20.4065697516636,22.8358151446688,-52.3537213810636));
#16991=CARTESIAN_POINT('Ctrl Pts',(-20.3890291622611,22.9179311394058,-52.3480838085983));
#16992=CARTESIAN_POINT('Ctrl Pts',(-20.3642192848365,23.0612775348118,-52.3384770604008));
#16993=CARTESIAN_POINT('Ctrl Pts',(-20.3554627844399,23.1222058838093,-52.3344662770859));
#16994=CARTESIAN_POINT('Ctrl Pts',(-20.3463670203406,23.2015809608084,-52.3293656008616));
#16995=CARTESIAN_POINT('Ctrl Pts',(-20.3444337465069,23.2198282789951,-52.3282015243654));
#16996=CARTESIAN_POINT('Ctrl Pts',(-20.3419298038576,23.245557432946,-52.326573052818));
#16997=CARTESIAN_POINT('Ctrl Pts',(-20.3412292932023,23.2530258730712,-52.326101883417));
#16998=CARTESIAN_POINT('Ctrl Pts',(-20.3402056436602,23.2643650975986,-52.3253889041492));
#16999=CARTESIAN_POINT('Ctrl Pts',(-20.3398634219571,23.2682340698776,-52.3251460559157));
#17000=CARTESIAN_POINT('Ctrl Pts',(-20.3393173055581,23.274537993742,-52.3247510682651));
#17001=CARTESIAN_POINT('Ctrl Pts',(-20.3391091853444,23.2769725613836,-52.3245986940545));
#17002=CARTESIAN_POINT('Ctrl Pts',(-20.338714196736,23.2816558503865,-52.324305906483));
#17003=CARTESIAN_POINT('Ctrl Pts',(-20.3385269210033,23.2839045341091,-52.3241654702888));
#17004=CARTESIAN_POINT('Ctrl Pts',(-20.3381920542471,23.2879771038951,-52.3239113941354));
#17005=CARTESIAN_POINT('Ctrl Pts',(-20.3380436552783,23.2898009140496,-52.3237977086767));
#17006=CARTESIAN_POINT('Ctrl Pts',(-20.3377465543131,23.2934911378986,-52.3235678784309));
#17007=CARTESIAN_POINT('Ctrl Pts',(-20.3375979260398,23.2953575477029,-52.3234517382075));
#17008=CARTESIAN_POINT('Ctrl Pts',(-20.3371815309458,23.300644679962,-52.3231230226498));
#17009=CARTESIAN_POINT('Ctrl Pts',(-20.3369175993968,23.3040657151614,-52.3229106646284));
#17010=CARTESIAN_POINT('Ctrl Pts',(-20.3358348848543,23.3183980914514,-52.3220223816247));
#17011=CARTESIAN_POINT('Ctrl Pts',(-20.3350661982722,23.329313310901,-52.321349253681));
#17012=CARTESIAN_POINT('Ctrl Pts',(-20.322096271135,23.5279132476972,-52.3091596615846));
#17013=CARTESIAN_POINT('Ctrl Pts',(-20.326290688331,23.7163390405978,-52.298523168509));
#17014=CARTESIAN_POINT('Ctrl Pts',(-20.3646203553982,24.0640733249256,-52.2789250280744));
#17015=CARTESIAN_POINT('Ctrl Pts',(-20.3944079082313,24.2232362328011,-52.2699634481087));
#17016=CARTESIAN_POINT('Ctrl Pts',(-20.4714891494131,24.5127199914436,-52.2528662552838));
#17017=CARTESIAN_POINT('Ctrl Pts',(-20.515474792628,24.6435249175556,-52.244823277502));
#17018=CARTESIAN_POINT('Ctrl Pts',(-20.5759133299923,24.7911773622757,-52.2351798070497));
#17019=CARTESIAN_POINT('Ctrl Pts',(-20.584333208839,24.8111691254856,-52.2338619399014));
#17020=CARTESIAN_POINT('Ctrl Pts',(-20.595390926387,24.8367003737058,-52.2321627343234));
#17021=CARTESIAN_POINT('Ctrl Pts',(-20.5978437798778,24.8423197583167,-52.2317877306516));
#17022=CARTESIAN_POINT('Ctrl Pts',(-20.6018147268672,24.8513466825338,-52.23118368707));
#17023=CARTESIAN_POINT('Ctrl Pts',(-20.6033227348869,24.8547586645989,-52.2309549934472));
#17024=CARTESIAN_POINT('Ctrl Pts',(-20.6062013011727,24.8612411743442,-52.2305197698409));
#17025=CARTESIAN_POINT('Ctrl Pts',(-20.6075707485103,24.8643121923923,-52.2303132782721));
#17026=CARTESIAN_POINT('Ctrl Pts',(-20.6106968881655,24.8712932409254,-52.2298431744942));
#17027=CARTESIAN_POINT('Ctrl Pts',(-20.6124565776214,24.8752019151794,-52.2295794593396));
#17028=CARTESIAN_POINT('Ctrl Pts',(-20.6178213201204,24.8870550085882,-52.2287781989981));
#17029=CARTESIAN_POINT('Ctrl Pts',(-20.6214508166278,24.8949882619648,-52.2282398111765));
#17030=CARTESIAN_POINT('Ctrl Pts',(-20.6472606716036,24.9508025621494,-52.2244369890565));
#17031=CARTESIAN_POINT('Ctrl Pts',(-20.6705807666726,24.9981448342399,-52.2211331809843));
#17032=CARTESIAN_POINT('Ctrl Pts',(-20.6969805598483,25.0485762345562,-52.2175255428149));
#17033=CARTESIAN_POINT('Ctrl Pts',(-20.6989167638517,25.0522575924858,-52.2172616812532));
#17034=CARTESIAN_POINT('Ctrl Pts',(-20.7027423416774,25.0594972140609,-52.2167417675745));
#17035=CARTESIAN_POINT('Ctrl Pts',(-20.704631272039,25.063055704571,-52.2164857310375));
#17036=CARTESIAN_POINT('Ctrl Pts',(-20.7088702718867,25.0710053786494,-52.2159126617132));
#17037=CARTESIAN_POINT('Ctrl Pts',(-20.7112238544829,25.075394668481,-52.2155955092694));
#17038=CARTESIAN_POINT('Ctrl Pts',(-20.7221355454589,25.0956315343891,-52.2141298458438));
#17039=CARTESIAN_POINT('Ctrl Pts',(-20.7308161055018,25.1114124107428,-52.2129771809979));
#17040=CARTESIAN_POINT('Ctrl Pts',(-20.7726327987351,25.1859469245321,-52.2074865919345));
#17041=CARTESIAN_POINT('Ctrl Pts',(-20.8074740740741,25.2437202371994,-52.2030922589324));
#17042=CARTESIAN_POINT('Ctrl Pts',(-20.9770113200173,25.5058726595033,-52.1825155827544));
#17043=CARTESIAN_POINT('Ctrl Pts',(-21.1328998420461,25.6955747959056,-52.1656974453406));
#17044=CARTESIAN_POINT('Ctrl Pts',(-21.3400442207299,25.896099281951,-52.1464586971225));
#17045=CARTESIAN_POINT('Ctrl Pts',(-21.3719773629991,25.925780962463,-52.1435696638877));
#17046=CARTESIAN_POINT('Ctrl Pts',(-21.4535301069519,25.9985560679456,-52.1364000406852));
#17047=CARTESIAN_POINT('Ctrl Pts',(-21.5038870243687,26.0407996175307,-52.1321583934052));
#17048=CARTESIAN_POINT('Ctrl Pts',(-21.5610949956279,26.0858827340856,-52.1275725973153));
#17049=CARTESIAN_POINT('Ctrl Pts',(-21.5667001824379,26.0902699148189,-52.1271256926731));
#17050=CARTESIAN_POINT('Ctrl Pts',(-21.5752718344897,26.0969332709644,-52.1264459928998));
#17051=CARTESIAN_POINT('Ctrl Pts',(-21.5782277576932,26.0992228793367,-52.1262122709998));
#17052=CARTESIAN_POINT('Ctrl Pts',(-21.5830738034972,26.1029630696163,-52.1258302066036));
#17053=CARTESIAN_POINT('Ctrl Pts',(-21.584961551617,26.1044167008118,-52.1256816500384));
#17054=CARTESIAN_POINT('Ctrl Pts',(-21.5886047667294,26.1072156718786,-52.1253954781903));
#17055=CARTESIAN_POINT('Ctrl Pts',(-21.5903600091168,26.1085613000153,-52.1252578424673));
#17056=CARTESIAN_POINT('Ctrl Pts',(-21.5935680325026,26.1110154399811,-52.1250067233921));
#17057=CARTESIAN_POINT('Ctrl Pts',(-21.595020365455,26.1121245187348,-52.1248931997333));
#17058=CARTESIAN_POINT('Ctrl Pts',(-21.5979838837376,26.1143836310927,-52.1246618837174));
#17059=CARTESIAN_POINT('Ctrl Pts',(-21.5994951364912,26.1155335599256,-52.1245440988558));
#17060=CARTESIAN_POINT('Ctrl Pts',(-21.6038452164394,26.1188375165349,-52.1242055608522));
#17061=CARTESIAN_POINT('Ctrl Pts',(-21.6066866125303,26.12098818115,-52.1239850465929));
#17062=CARTESIAN_POINT('Ctrl Pts',(-21.6191517413112,26.1303906100946,-52.1230203096895));
#17063=CARTESIAN_POINT('Ctrl Pts',(-21.628812698336,26.1375932019244,-52.1222795167671));
#17064=CARTESIAN_POINT('Ctrl Pts',(-21.776591904548,26.2464836992793,-52.1110490172245));
#17065=CARTESIAN_POINT('Ctrl Pts',(-21.9225646111997,26.3370355473912,-52.1012875088868));
#17066=CARTESIAN_POINT('Ctrl Pts',(-22.0750360382923,26.4155367863704,-52.0916569661403));
#17067=CARTESIAN_POINT('Origin',(-23.5502525316942,23.5502525316942,-77.3107734492734));
#17068=CARTESIAN_POINT('',(-22.0750357068451,26.4155366157218,-50.5964032705492));
#17069=CARTESIAN_POINT('',(-22.0750360284016,26.415536781278,-50.8458393738826));
#17070=CARTESIAN_POINT('',(-22.0750360153461,26.4155367745563,-77.3107734492734));
#17071=CARTESIAN_POINT('',(-26.7730025211998,23.5499924521692,-51.4361781865152));
#17072=CARTESIAN_POINT('Ctrl Pts',(-22.0750357068432,26.4155366157209,-50.5964032705493));
#17073=CARTESIAN_POINT('Ctrl Pts',(-21.8523485774069,26.300884179736,-50.6104004212466));
#17074=CARTESIAN_POINT('Ctrl Pts',(-21.6435050826592,26.1605201296056,-50.6245125474874));
#17075=CARTESIAN_POINT('Ctrl Pts',(-21.4370245485272,25.9835258314191,-50.6409549397257));
#17076=CARTESIAN_POINT('Ctrl Pts',(-21.4213415961363,25.9698164710839,-50.6422204904967));
#17077=CARTESIAN_POINT('Ctrl Pts',(-21.4010854162771,25.9517599837174,-50.6438774603741));
#17078=CARTESIAN_POINT('Ctrl Pts',(-21.3963902605948,25.9475498950503,-50.6442631151753));
#17079=CARTESIAN_POINT('Ctrl Pts',(-21.3891884037849,25.9410538422488,-50.6448571289976));
#17080=CARTESIAN_POINT('Ctrl Pts',(-21.3866728861307,25.9387776390878,-50.6450650749099));
#17081=CARTESIAN_POINT('Ctrl Pts',(-21.3817365449963,25.9342967215347,-50.6454740552082));
#17082=CARTESIAN_POINT('Ctrl Pts',(-21.3793154776693,25.9320922809241,-50.6456750778362));
#17083=CARTESIAN_POINT('Ctrl Pts',(-21.3739985830968,25.9272362780307,-50.6461175031256));
#17084=CARTESIAN_POINT('Ctrl Pts',(-21.3711042367558,25.9245831084216,-50.6463589741065));
#17085=CARTESIAN_POINT('Ctrl Pts',(-21.3651225139799,25.9190796727348,-50.6468593281617));
#17086=CARTESIAN_POINT('Ctrl Pts',(-21.3620358503229,25.9162286460172,-50.6471182435472));
#17087=CARTESIAN_POINT('Ctrl Pts',(-21.3541715954455,25.9089361975631,-50.6477797713994));
#17088=CARTESIAN_POINT('Ctrl Pts',(-21.3494019140452,25.9044863076776,-50.6481827472665));
#17089=CARTESIAN_POINT('Ctrl Pts',(-21.3357215758627,25.8916452837271,-50.6493436510699));
#17090=CARTESIAN_POINT('Ctrl Pts',(-21.3268452425592,25.8832178965395,-50.6501031434403));
#17091=CARTESIAN_POINT('Ctrl Pts',(-21.2414001677347,25.8011638974573,-50.6574754240567));
#17092=CARTESIAN_POINT('Ctrl Pts',(-21.1684758028635,25.7238524454953,-50.6642502535098));
#17093=CARTESIAN_POINT('Ctrl Pts',(-20.9549644604765,25.4738272077129,-50.6856760461208));
#17094=CARTESIAN_POINT('Ctrl Pts',(-20.8283594836573,25.29006164396,-50.7008133803542));
#17095=CARTESIAN_POINT('Ctrl Pts',(-20.6428144723012,24.950260983726,-50.7269526814135));
#17096=CARTESIAN_POINT('Ctrl Pts',(-20.5750932149337,24.7999170641754,-50.737949783234));
#17097=CARTESIAN_POINT('Ctrl Pts',(-20.5159184055842,24.6360815484909,-50.7489062931017));
#17098=CARTESIAN_POINT('Ctrl Pts',(-20.5127231878534,24.6271108015433,-50.7495030229306));
#17099=CARTESIAN_POINT('Ctrl Pts',(-20.5084921676235,24.6150633065856,-50.7503000203109));
#17100=CARTESIAN_POINT('Ctrl Pts',(-20.5074212254287,24.6119990836494,-50.7505023524568));
#17101=CARTESIAN_POINT('Ctrl Pts',(-20.5057521360045,24.6072001510443,-50.7508186274262));
#17102=CARTESIAN_POINT('Ctrl Pts',(-20.5051508414509,24.6054665505182,-50.750932758236));
#17103=CARTESIAN_POINT('Ctrl Pts',(-20.5039998343296,24.602138889382,-50.751151596795));
#17104=CARTESIAN_POINT('Ctrl Pts',(-20.5034498957715,24.6005449211943,-50.7512563174541));
#17105=CARTESIAN_POINT('Ctrl Pts',(-20.5021520115566,24.5967734738717,-50.7515038486648));
#17106=CARTESIAN_POINT('Ctrl Pts',(-20.5014051489639,24.5945956267435,-50.7516465938053));
#17107=CARTESIAN_POINT('Ctrl Pts',(-20.4992215740068,24.5882060280696,-50.7520648328016));
#17108=CARTESIAN_POINT('Ctrl Pts',(-20.4977912431168,24.5839920770854,-50.7523399467391));
#17109=CARTESIAN_POINT('Ctrl Pts',(-20.4872539421143,24.5527351791487,-50.7543753940437));
#17110=CARTESIAN_POINT('Ctrl Pts',(-20.4784973996368,24.5255742031726,-50.7561152636928));
#17111=CARTESIAN_POINT('Ctrl Pts',(-20.4506255884674,24.4350202791087,-50.7618316675569));
#17112=CARTESIAN_POINT('Ctrl Pts',(-20.4331019729121,24.3711513177017,-50.7657275692437));
#17113=CARTESIAN_POINT('Ctrl Pts',(-20.3743734820889,24.1279643427228,-50.7802080043999));
#17114=CARTESIAN_POINT('Ctrl Pts',(-20.3465767972757,23.9457644941269,-50.7903563699776));
#17115=CARTESIAN_POINT('Ctrl Pts',(-20.3195256562256,23.5352883572622,-50.8134044793081));
#17116=CARTESIAN_POINT('Ctrl Pts',(-20.3286280083119,23.3074920722334,-50.8263549843491));
#17117=CARTESIAN_POINT('Ctrl Pts',(-20.3636584581088,23.0686578907003,-50.8410093998726));
#17118=CARTESIAN_POINT('Ctrl Pts',(-20.3657895074648,23.0547624454579,-50.8418656753381));
#17119=CARTESIAN_POINT('Ctrl Pts',(-20.3688608738422,23.0355744096435,-50.8430533238444));
#17120=CARTESIAN_POINT('Ctrl Pts',(-20.3697236427263,23.0302694205698,-50.8433822309543));
#17121=CARTESIAN_POINT('Ctrl Pts',(-20.371122273503,23.0218032492617,-50.8439080223152));
#17122=CARTESIAN_POINT('Ctrl Pts',(-20.3716495918545,23.0186406494224,-50.8441046344678));
#17123=CARTESIAN_POINT('Ctrl Pts',(-20.3727313470763,23.0122119583332,-50.8445046994295));
#17124=CARTESIAN_POINT('Ctrl Pts',(-20.373286102112,23.0089459249933,-50.8447081621604));
#17125=CARTESIAN_POINT('Ctrl Pts',(-20.3745753363711,23.001426012113,-50.8451771218889));
#17126=CARTESIAN_POINT('Ctrl Pts',(-20.3753133274638,22.9971727484424,-50.8454427304903));
#17127=CARTESIAN_POINT('Ctrl Pts',(-20.3768799635295,22.9882502231419,-50.846000697158));
#17128=CARTESIAN_POINT('Ctrl Pts',(-20.3777103728771,22.9835812854327,-50.8462931109964));
#17129=CARTESIAN_POINT('Ctrl Pts',(-20.3799356155677,22.9712281746823,-50.8470679645034));
#17130=CARTESIAN_POINT('Ctrl Pts',(-20.3813480744009,22.9635472449331,-50.8475509661928));
#17131=CARTESIAN_POINT('Ctrl Pts',(-20.385675601702,22.940485793652,-50.8490048282376));
#17132=CARTESIAN_POINT('Ctrl Pts',(-20.388674798009,22.9251214729749,-50.849978370961));
#17133=CARTESIAN_POINT('Ctrl Pts',(-20.4242875329017,22.7494986262119,-50.8611640393299));
#17134=CARTESIAN_POINT('Ctrl Pts',(-20.468937090516,22.59194969029,-50.8717667387811));
#17135=CARTESIAN_POINT('Ctrl Pts',(-20.6342037865814,22.1422883491935,-50.903647855608));
#17136=CARTESIAN_POINT('Ctrl Pts',(-20.7859736658164,21.8636991125608,-50.925660281041));
#17137=CARTESIAN_POINT('Ctrl Pts',(-20.985644326228,21.5985430261241,-50.946669475454));
#17138=CARTESIAN_POINT('Ctrl Pts',(-20.9955858337069,21.5855481440441,-50.9476987560067));
#17139=CARTESIAN_POINT('Ctrl Pts',(-21.0078341708892,21.5697880940986,-50.9489460505656));
#17140=CARTESIAN_POINT('Ctrl Pts',(-21.0100469908302,21.5669506584499,-50.949170573052));
#17141=CARTESIAN_POINT('Ctrl Pts',(-21.0136998621713,21.5622828284069,-50.9495398576055));
#17142=CARTESIAN_POINT('Ctrl Pts',(-21.0151371456787,21.5604502887286,-50.9496848157399));
#17143=CARTESIAN_POINT('Ctrl Pts',(-21.017730332841,21.5571513397717,-50.9499457334934));
#17144=CARTESIAN_POINT('Ctrl Pts',(-21.0188855217576,21.5556843804415,-50.9500617437598));
#17145=CARTESIAN_POINT('Ctrl Pts',(-21.0213702446299,21.5525346988116,-50.9503107983834));
#17146=CARTESIAN_POINT('Ctrl Pts',(-21.0227001798117,21.5508523040752,-50.9504438128606));
#17147=CARTESIAN_POINT('Ctrl Pts',(-21.0263419279145,21.5462548599001,-50.9508072548323));
#17148=CARTESIAN_POINT('Ctrl Pts',(-21.0286571201018,21.5433424726742,-50.951037439623));
#17149=CARTESIAN_POINT('Ctrl Pts',(-21.0406354140028,21.5283278735181,-50.9522239290978));
#17150=CARTESIAN_POINT('Ctrl Pts',(-21.0503808302072,21.5162911506554,-50.9531743893107));
#17151=CARTESIAN_POINT('Ctrl Pts',(-21.1091696163747,21.4447410114492,-50.9588231579699));
#17152=CARTESIAN_POINT('Ctrl Pts',(-21.1602537452573,21.3869281243936,-50.9633830750513));
#17153=CARTESIAN_POINT('Ctrl Pts',(-21.3354527836962,21.2024426561269,-50.9781348699519));
#17154=CARTESIAN_POINT('Ctrl Pts',(-21.4679465270699,21.0841706650467,-50.9879376692314));
#17155=CARTESIAN_POINT('Ctrl Pts',(-21.6909237986502,20.9159755506486,-51.0035684909384));
#17156=CARTESIAN_POINT('Ctrl Pts',(-21.7752094530078,20.8584614589602,-51.0093036930626));
#17157=CARTESIAN_POINT('Ctrl Pts',(-21.9809378944934,20.7319481042448,-51.0231414855137));
#17158=CARTESIAN_POINT('Ctrl Pts',(-22.1044058459751,20.6666596527171,-51.0313277318296));
#17159=CARTESIAN_POINT('Ctrl Pts',(-22.241767387936,20.6050690388056,-51.0404851119107));
#17160=CARTESIAN_POINT('Ctrl Pts',(-22.2518530865624,20.600608815182,-51.0411577085419));
#17161=CARTESIAN_POINT('Ctrl Pts',(-22.2659617965919,20.5944558679757,-51.0420989672463));
#17162=CARTESIAN_POINT('Ctrl Pts',(-22.2699657355052,20.5927193824771,-51.0423661308483));
#17163=CARTESIAN_POINT('Ctrl Pts',(-22.2768891591874,20.5897334271074,-51.0428281748131));
#17164=CARTESIAN_POINT('Ctrl Pts',(-22.2798069938948,20.5884801261164,-51.0430229240539));
#17165=CARTESIAN_POINT('Ctrl Pts',(-22.2857902938033,20.5859205808457,-51.0434223265646));
#17166=CARTESIAN_POINT('Ctrl Pts',(-22.2888559407207,20.5846147746471,-51.0436269944535));
#17167=CARTESIAN_POINT('Ctrl Pts',(-22.2959923437172,20.5815881054206,-51.0441034988086));
#17168=CARTESIAN_POINT('Ctrl Pts',(-22.3000646181626,20.5798708600037,-51.0443754581047));
#17169=CARTESIAN_POINT('Ctrl Pts',(-22.3086447560199,20.5762734548074,-51.0449485766859));
#17170=CARTESIAN_POINT('Ctrl Pts',(-22.3131533835322,20.5743951568236,-51.0452497985681));
#17171=CARTESIAN_POINT('Ctrl Pts',(-22.3251977049797,20.5694095844722,-51.0460546598658));
#17172=CARTESIAN_POINT('Ctrl Pts',(-22.3327409104562,20.5663206533419,-51.0465589208699));
#17173=CARTESIAN_POINT('Ctrl Pts',(-22.3556723035424,20.5570317116574,-51.0480924866962));
#17174=CARTESIAN_POINT('Ctrl Pts',(-22.371096538562,20.5509219520077,-51.0491248334637));
#17175=CARTESIAN_POINT('Ctrl Pts',(-22.4268255253841,20.5293432200067,-51.0528581423542));
#17176=CARTESIAN_POINT('Ctrl Pts',(-22.4673915138064,20.5145659482325,-51.0555820482971));
#17177=CARTESIAN_POINT('Ctrl Pts',(-22.6046486360784,20.467667502468,-51.0648232969655));
#17178=CARTESIAN_POINT('Ctrl Pts',(-22.7025555605314,20.4393196186817,-51.071458307535));
#17179=CARTESIAN_POINT('Ctrl Pts',(-23.1063876117426,20.3428744107995,-51.098954591283));
#17180=CARTESIAN_POINT('Ctrl Pts',(-23.4200966646547,20.3149267546062,-51.1208013398413));
#17181=CARTESIAN_POINT('Ctrl Pts',(-23.7664128039007,20.3345847012311,-51.1430487047743));
#17182=CARTESIAN_POINT('Ctrl Pts',(-23.7999039736679,20.3370112961244,-51.1451784966865));
#17183=CARTESIAN_POINT('Ctrl Pts',(-23.8383957820652,20.3404057035389,-51.1475966351376));
#17184=CARTESIAN_POINT('Ctrl Pts',(-23.8434378498833,20.3408623150043,-51.1479128018672));
#17185=CARTESIAN_POINT('Ctrl Pts',(-23.850869208306,20.3415529603178,-51.1483779046328));
#17186=CARTESIAN_POINT('Ctrl Pts',(-23.8532593153964,20.3417777827319,-51.1485273578818));
#17187=CARTESIAN_POINT('Ctrl Pts',(-23.8575197968318,20.3421833427278,-51.1487935217528));
#17188=CARTESIAN_POINT('Ctrl Pts',(-23.8593902642088,20.3423630454699,-51.1489102910642));
#17189=CARTESIAN_POINT('Ctrl Pts',(-23.8633271120795,20.3427447483386,-51.1491558826757));
#17190=CARTESIAN_POINT('Ctrl Pts',(-23.8653934498348,20.3429471089222,-51.1492846839897));
#17191=CARTESIAN_POINT('Ctrl Pts',(-23.8708576454707,20.3434875600743,-51.1496250164038));
#17192=CARTESIAN_POINT('Ctrl Pts',(-23.8742551757371,20.3438290554363,-51.149836354296));
#17193=CARTESIAN_POINT('Ctrl Pts',(-23.8896688765324,20.3454030790208,-51.1507939204927));
#17194=CARTESIAN_POINT('Ctrl Pts',(-23.9016788080628,20.3466977791373,-51.1515366695742));
#17195=CARTESIAN_POINT('Ctrl Pts',(-24.1830996645291,20.3786372900485,-51.1688681407623));
#17196=CARTESIAN_POINT('Ctrl Pts',(-24.4476342174609,20.4430994449741,-51.1836520011355));
#17197=CARTESIAN_POINT('Ctrl Pts',(-24.7796606343943,20.5700236047337,-51.2035742041776));
#17198=CARTESIAN_POINT('Ctrl Pts',(-24.8571071608163,20.6031626371346,-51.2083197648294));
#17199=CARTESIAN_POINT('Ctrl Pts',(-25.063821796896,20.7013668172127,-51.2214090449272));
#17200=CARTESIAN_POINT('Ctrl Pts',(-25.1901350865688,20.7721563426756,-51.2298822940286));
#17201=CARTESIAN_POINT('Ctrl Pts',(-25.3205620314773,20.857253223562,-51.2393551503458));
#17202=CARTESIAN_POINT('Ctrl Pts',(-25.3298353183021,20.8633721660326,-51.2400327365532));
#17203=CARTESIAN_POINT('Ctrl Pts',(-25.3427185408006,20.871969063205,-51.2409798590476));
#17204=CARTESIAN_POINT('Ctrl Pts',(-25.3463554219401,20.8744066581942,-51.2412478720568));
#17205=CARTESIAN_POINT('Ctrl Pts',(-25.3526246396796,20.8786270986313,-51.2417109884189));
#17206=CARTESIAN_POINT('Ctrl Pts',(-25.3552593331547,20.8804064468412,-51.2419059592086));
#17207=CARTESIAN_POINT('Ctrl Pts',(-25.3606482592205,20.884057497316,-51.2423054500769));
#17208=CARTESIAN_POINT('Ctrl Pts',(-25.3634022312676,20.8859295748447,-51.242509984226));
#17209=CARTESIAN_POINT('Ctrl Pts',(-25.369794000597,20.8902890307971,-51.242985573136));
#17210=CARTESIAN_POINT('Ctrl Pts',(-25.3734296008231,20.8927796047472,-51.2432567493032));
#17211=CARTESIAN_POINT('Ctrl Pts',(-25.3810692196801,20.8980361942621,-51.2438279863253));
#17212=CARTESIAN_POINT('Ctrl Pts',(-25.3850721012694,20.9008038357887,-51.2441281088905));
#17213=CARTESIAN_POINT('Ctrl Pts',(-25.3957277470957,20.9082070098693,-51.2449292189247));
#17214=CARTESIAN_POINT('Ctrl Pts',(-25.4023692793907,20.9128585791288,-51.2454308203781));
#17215=CARTESIAN_POINT('Ctrl Pts',(-25.4224498126903,20.927035756903,-51.2469543730466));
#17216=CARTESIAN_POINT('Ctrl Pts',(-25.4358332418582,20.936639271146,-51.2479793197093));
#17217=CARTESIAN_POINT('Ctrl Pts',(-25.5972046479728,21.0543187514229,-51.2604549166099));
#17218=CARTESIAN_POINT('Ctrl Pts',(-25.7357621252395,21.1747050699207,-51.2723999740091));
#17219=CARTESIAN_POINT('Ctrl Pts',(-26.0688852696336,21.5180723732423,-51.3044084450203));
#17220=CARTESIAN_POINT('Ctrl Pts',(-26.2443585050461,21.7571912446087,-51.3249072531888));
#17221=CARTESIAN_POINT('Ctrl Pts',(-26.3922382351895,22.0305560530528,-51.3445658413584));
#17222=CARTESIAN_POINT('Ctrl Pts',(-26.3995493922707,22.0443084591247,-51.3455452349742));
#17223=CARTESIAN_POINT('Ctrl Pts',(-26.4083971639271,22.0612463814005,-51.3467392656973));
#17224=CARTESIAN_POINT('Ctrl Pts',(-26.4100284452235,22.0643818175785,-51.3469597856966));
#17225=CARTESIAN_POINT('Ctrl Pts',(-26.4127169242311,22.069570089161,-51.347323832487));
#17226=CARTESIAN_POINT('Ctrl Pts',(-26.4137770738864,22.0716213773827,-51.3474675459373));
#17227=CARTESIAN_POINT('Ctrl Pts',(-26.4156044220633,22.0751664573148,-51.3477155327629));
#17228=CARTESIAN_POINT('Ctrl Pts',(-26.4163726562595,22.0766597066307,-51.3478198721848));
#17229=CARTESIAN_POINT('Ctrl Pts',(-26.4180961413374,22.0800161639207,-51.3480541384553));
#17230=CARTESIAN_POINT('Ctrl Pts',(-26.4190507421148,22.0818796994603,-51.3481840235282));
#17231=CARTESIAN_POINT('Ctrl Pts',(-26.4215930542813,22.0868546474855,-51.3485302874222));
#17232=CARTESIAN_POINT('Ctrl Pts',(-26.4231775299967,22.0899677243499,-51.3487464607814));
#17233=CARTESIAN_POINT('Ctrl Pts',(-26.430579009352,22.1045683527065,-51.3497580150938));
#17234=CARTESIAN_POINT('Ctrl Pts',(-26.4363323004514,22.1160883343945,-51.3505494175845));
#17235=CARTESIAN_POINT('Ctrl Pts',(-26.5720887719039,22.3920428999539,-51.369354339184));
#17236=CARTESIAN_POINT('Ctrl Pts',(-26.6653106962469,22.6730842376335,-51.3852574007824));
#17237=CARTESIAN_POINT('Ctrl Pts',(-26.754926724025,23.1565857376758,-51.4129306387781));
#17238=CARTESIAN_POINT('Ctrl Pts',(-26.7729866310584,23.3530913192336,-51.4242445420252));
#17239=CARTESIAN_POINT('Ctrl Pts',(-26.7730025211998,23.5499924521692,-51.4361781865152));
#17240=CARTESIAN_POINT('Ctrl Pts',(-26.7730025212924,23.5499936018635,-51.436178256195));
#17241=CARTESIAN_POINT('Ctrl Pts',(-26.7730036694541,23.564284106563,-51.4370443651463));
#17242=CARTESIAN_POINT('Ctrl Pts',(-26.7729097659511,23.5785743256242,-51.4379134002376));
#17243=CARTESIAN_POINT('Ctrl Pts',(-26.772653767245,23.5979343931753,-51.4390948872342));
#17244=CARTESIAN_POINT('Ctrl Pts',(-26.7725747424517,23.6030052793834,-51.4394047328048));
#17245=CARTESIAN_POINT('Ctrl Pts',(-26.7724192226876,23.6116716775646,-51.4399349394188));
#17246=CARTESIAN_POINT('Ctrl Pts',(-26.7723486780014,23.6152672978123,-51.4401551136329));
#17247=CARTESIAN_POINT('Ctrl Pts',(-26.7722054168766,23.6219950120331,-51.4405674475457));
#17248=CARTESIAN_POINT('Ctrl Pts',(-26.7721341514057,23.6251271353701,-51.4407595614916));
#17249=CARTESIAN_POINT('Ctrl Pts',(-26.771979449176,23.6315166008643,-51.4411517772963));
#17250=CARTESIAN_POINT('Ctrl Pts',(-26.7718956393233,23.6347739296146,-51.4413518906462));
#17251=CARTESIAN_POINT('Ctrl Pts',(-26.7716885671897,23.6423736663668,-51.4418191618513));
#17252=CARTESIAN_POINT('Ctrl Pts',(-26.7715614646836,23.646715955801,-51.4420864400082));
#17253=CARTESIAN_POINT('Ctrl Pts',(-26.7712073090244,23.6580327738193,-51.4427837835971));
#17254=CARTESIAN_POINT('Ctrl Pts',(-26.770966382813,23.6650068178115,-51.4432142841619));
#17255=CARTESIAN_POINT('Ctrl Pts',(-26.7698809013161,23.6937245739015,-51.4449901683132));
#17256=CARTESIAN_POINT('Ctrl Pts',(-26.7688388009666,23.7154598414678,-51.4463417437686));
#17257=CARTESIAN_POINT('Ctrl Pts',(-26.745420974231,24.1185132049987,-51.4715484643977));
#17258=CARTESIAN_POINT('Ctrl Pts',(-26.6556390275667,24.4928170257909,-51.4978802048695));
#17259=CARTESIAN_POINT('Ctrl Pts',(-26.4702590529652,24.9163303656281,-51.5286790372521));
#17260=CARTESIAN_POINT('Ctrl Pts',(-26.4351990352113,24.9888951366271,-51.5339734477163));
#17261=CARTESIAN_POINT('Ctrl Pts',(-26.3824906048417,25.0882919125751,-51.5411778603223));
#17262=CARTESIAN_POINT('Ctrl Pts',(-26.3671083522227,25.1162860940888,-51.5432013611107));
#17263=CARTESIAN_POINT('Ctrl Pts',(-26.3490490468443,25.148024906892,-51.5454851256712));
#17264=CARTESIAN_POINT('Ctrl Pts',(-26.3467778555827,25.1519967714617,-51.5457707324011));
#17265=CARTESIAN_POINT('Ctrl Pts',(-26.3433380859656,25.1579826304651,-51.546200859667));
#17266=CARTESIAN_POINT('Ctrl Pts',(-26.3421757831382,25.1600001958026,-51.5463457846553));
#17267=CARTESIAN_POINT('Ctrl Pts',(-26.3401664370759,25.1634793653379,-51.5465956074293));
#17268=CARTESIAN_POINT('Ctrl Pts',(-26.3393204323216,25.1649415611888,-51.5467005727758));
#17269=CARTESIAN_POINT('Ctrl Pts',(-26.3375592362298,25.1679800178544,-51.5469186329217));
#17270=CARTESIAN_POINT('Ctrl Pts',(-26.3366438598279,25.1695561632495,-51.5470317150025));
#17271=CARTESIAN_POINT('Ctrl Pts',(-26.3341252902424,25.1738843158271,-51.5473421548982));
#17272=CARTESIAN_POINT('Ctrl Pts',(-26.3325193483289,25.176634733852,-51.5475393332184));
#17273=CARTESIAN_POINT('Ctrl Pts',(-26.3263129569081,25.1872280209547,-51.5482984113393));
#17274=CARTESIAN_POINT('Ctrl Pts',(-26.3216833441406,25.1950538854765,-51.5488584282042));
#17275=CARTESIAN_POINT('Ctrl Pts',(-26.2447018885549,25.3239349518066,-51.5580703769067));
#17276=CARTESIAN_POINT('Ctrl Pts',(-26.1645029373227,25.4401500692814,-51.5662224541106));
#17277=CARTESIAN_POINT('Ctrl Pts',(-25.9575071527404,25.7015914472988,-51.58510858733));
#17278=CARTESIAN_POINT('Ctrl Pts',(-25.8248110361358,25.8414356486262,-51.5956817586266));
#17279=CARTESIAN_POINT('Ctrl Pts',(-25.5642414380616,26.0709549655142,-51.6153880568697));
#17280=CARTESIAN_POINT('Ctrl Pts',(-25.4408419877386,26.1647800380138,-51.6243689863156));
#17281=CARTESIAN_POINT('Ctrl Pts',(-25.298435692277,26.2576876767086,-51.6346380324984));
#17282=CARTESIAN_POINT('Ctrl Pts',(-25.2856240598996,26.2659172890256,-51.6355609552479));
#17283=CARTESIAN_POINT('Ctrl Pts',(-25.266287114674,26.2781457538515,-51.6369527610517));
#17284=CARTESIAN_POINT('Ctrl Pts',(-25.2598049717878,26.2822127390288,-51.6374191242336));
#17285=CARTESIAN_POINT('Ctrl Pts',(-25.2493382308296,26.2887278774802,-51.6381718693823));
#17286=CARTESIAN_POINT('Ctrl Pts',(-25.2453626549264,26.2911905284825,-51.6384577162642));
#17287=CARTESIAN_POINT('Ctrl Pts',(-25.2377478016283,26.2958846082984,-51.639005107057));
#17288=CARTESIAN_POINT('Ctrl Pts',(-25.2341094205912,26.2981174780778,-51.6392665972251));
#17289=CARTESIAN_POINT('Ctrl Pts',(-25.2276431156204,26.3020681758735,-51.639731239886));
#17290=CARTESIAN_POINT('Ctrl Pts',(-25.2248169569995,26.3037888935321,-51.6399342857869));
#17291=CARTESIAN_POINT('Ctrl Pts',(-25.2192325960557,26.3071771762468,-51.6403354374103));
#17292=CARTESIAN_POINT('Ctrl Pts',(-25.2164745315431,26.3088449622772,-51.6405335347295));
#17293=CARTESIAN_POINT('Ctrl Pts',(-25.2098233058674,26.3128533068648,-51.6410111930357));
#17294=CARTESIAN_POINT('Ctrl Pts',(-25.2059276965522,26.3151897725022,-51.6412909035125));
#17295=CARTESIAN_POINT('Ctrl Pts',(-25.1916268140821,26.3237259376996,-51.6423175439621));
#17296=CARTESIAN_POINT('Ctrl Pts',(-25.1811916536026,26.3298751396929,-51.6430663138612));
#17297=CARTESIAN_POINT('Ctrl Pts',(-25.0003776997322,26.4350559497767,-51.6560352379119));
#17298=CARTESIAN_POINT('Ctrl Pts',(-24.8213368479422,26.5182943918469,-51.6688360912537));
#17299=CARTESIAN_POINT('Ctrl Pts',(-24.5405378854017,26.61875363175,-51.6887796924346));
#17300=CARTESIAN_POINT('Ctrl Pts',(-24.4436780041307,26.6483412555545,-51.6956288440029));
#17301=CARTESIAN_POINT('Ctrl Pts',(-24.2700465053489,26.692559187397,-51.7077572734322));
#17302=CARTESIAN_POINT('Ctrl Pts',(-24.1938283139689,26.709050595567,-51.7130310825922));
#17303=CARTESIAN_POINT('Ctrl Pts',(-23.9917732260967,26.7451518347319,-51.7267844979734));
#17304=CARTESIAN_POINT('Ctrl Pts',(-23.865226894629,26.7601001402267,-51.7351713682567));
#17305=CARTESIAN_POINT('Ctrl Pts',(-23.7301585549299,26.76798696434,-51.7436663171584));
#17306=CARTESIAN_POINT('Ctrl Pts',(-23.7222020128434,26.7684219547318,-51.7441650439996));
#17307=CARTESIAN_POINT('Ctrl Pts',(-23.7113305142686,26.7689758741898,-51.7448441010364));
#17308=CARTESIAN_POINT('Ctrl Pts',(-23.7084169752362,26.7691203576474,-51.7450258531578));
#17309=CARTESIAN_POINT('Ctrl Pts',(-23.7035391603307,26.769355611517,-51.7453297446951));
#17310=CARTESIAN_POINT('Ctrl Pts',(-23.7015749977616,26.7694485400722,-51.745452006065));
#17311=CARTESIAN_POINT('Ctrl Pts',(-23.6977043824371,26.7696281165326,-51.745692723252));
#17312=CARTESIAN_POINT('Ctrl Pts',(-23.6957979376536,26.7697148686969,-51.745811184782));
#17313=CARTESIAN_POINT('Ctrl Pts',(-23.6915918973804,26.7699025195815,-51.7460723142505));
#17314=CARTESIAN_POINT('Ctrl Pts',(-23.6892922645835,26.770002648326,-51.7462149385553));
#17315=CARTESIAN_POINT('Ctrl Pts',(-23.6812458298729,26.7703443630428,-51.746713474016));
#17316=CARTESIAN_POINT('Ctrl Pts',(-23.6754984460422,26.7705730295073,-51.7470686595638));
#17317=CARTESIAN_POINT('Ctrl Pts',(-23.6168146182565,26.7727504927695,-51.7506863134718));
#17318=CARTESIAN_POINT('Ctrl Pts',(-23.5638346141267,26.773409361336,-51.7538777836002));
#17319=CARTESIAN_POINT('Ctrl Pts',(-23.4924288516575,26.7725364573219,-51.7581075298641));
#17320=CARTESIAN_POINT('Ctrl Pts',(-23.4740008345274,26.772153054801,-51.7591926816894));
#17321=CARTESIAN_POINT('Ctrl Pts',(-23.4016341088597,26.7700261961374,-51.7634322605402));
#17322=CARTESIAN_POINT('Ctrl Pts',(-23.3477373517381,26.7670860678997,-51.7665422522284));
#17323=CARTESIAN_POINT('Ctrl Pts',(-23.2302324153437,26.7577108519871,-51.7732661465508));
#17324=CARTESIAN_POINT('Ctrl Pts',(-23.1666906349007,26.7507341331022,-51.7768659469478));
#17325=CARTESIAN_POINT('Ctrl Pts',(-22.9562308121514,26.721267845123,-51.7887809163077));
#17326=CARTESIAN_POINT('Ctrl Pts',(-22.8106692946528,26.6905098000263,-51.7970167334664));
#17327=CARTESIAN_POINT('Ctrl Pts',(-22.518633440772,26.6073619704652,-51.8142476960407));
#17328=CARTESIAN_POINT('Ctrl Pts',(-22.3727933997389,26.5542060149213,-51.8232399775527));
#17329=CARTESIAN_POINT('Ctrl Pts',(-22.2174526948579,26.484531718338,-51.8335220374645));
#17330=CARTESIAN_POINT('Ctrl Pts',(-22.2035940315537,26.4781973095084,-51.834445596212));
#17331=CARTESIAN_POINT('Ctrl Pts',(-22.1828403447308,26.4685328630459,-51.8358382788749));
#17332=CARTESIAN_POINT('Ctrl Pts',(-22.1759112844077,26.4652760849147,-51.8363048791042));
#17333=CARTESIAN_POINT('Ctrl Pts',(-22.1647672318393,26.45998962148,-51.8370579613755));
#17334=CARTESIAN_POINT('Ctrl Pts',(-22.1605449104506,26.4579753821192,-51.8373439076827));
#17335=CARTESIAN_POINT('Ctrl Pts',(-22.1524767292414,26.4541049048096,-51.8378914882975));
#17336=CARTESIAN_POINT('Ctrl Pts',(-22.1486301411065,26.4522502010068,-51.838153068823));
#17337=CARTESIAN_POINT('Ctrl Pts',(-22.1418095704548,26.448944812103,-51.8386178108513));
#17338=CARTESIAN_POINT('Ctrl Pts',(-22.1388341086926,26.4474971790524,-51.8388208655916));
#17339=CARTESIAN_POINT('Ctrl Pts',(-22.1329650974872,26.444630578436,-51.8392220034561));
#17340=CARTESIAN_POINT('Ctrl Pts',(-22.1300714359481,26.4432118476508,-51.8394200781282));
#17341=CARTESIAN_POINT('Ctrl Pts',(-22.1231054100691,26.4397835106682,-51.8398976305233));
#17342=CARTESIAN_POINT('Ctrl Pts',(-22.119035163781,26.4377696365212,-51.8401772575919));
#17343=CARTESIAN_POINT('Ctrl Pts',(-22.1065408601127,26.4315548040674,-51.8410374535993));
#17344=CARTESIAN_POINT('Ctrl Pts',(-22.0981309981334,26.427325562431,-51.84161901497));
#17345=CARTESIAN_POINT('Ctrl Pts',(-22.0848319909862,26.4205644510068,-51.842542785673));
#17346=CARTESIAN_POINT('Ctrl Pts',(-22.0799306944496,26.4180568426721,-51.8428841275687));
#17347=CARTESIAN_POINT('Ctrl Pts',(-22.0750360141197,26.4155367739249,-51.843225903739));
#17348=CARTESIAN_POINT('Ctrl Pts',(-22.0750360382923,26.4155367863703,-52.0916569661403));
#17349=CARTESIAN_POINT('Ctrl Pts',(-22.0944602758593,26.4255375238482,-52.0904300742972));
#17350=CARTESIAN_POINT('Ctrl Pts',(-22.1139899917392,26.435342689167,-52.0892054490706));
#17351=CARTESIAN_POINT('Ctrl Pts',(-22.2686975094169,26.5110546796618,-52.079564296515));
#17352=CARTESIAN_POINT('Ctrl Pts',(-22.4082323090169,26.567622372871,-52.0712164686481));
#17353=CARTESIAN_POINT('Ctrl Pts',(-22.6571165825054,26.648774172461,-52.0562980725477));
#17354=CARTESIAN_POINT('Ctrl Pts',(-22.7647416847825,26.6777910699522,-52.0498402380234));
#17355=CARTESIAN_POINT('Ctrl Pts',(-22.9221673782742,26.7115955183053,-52.0402484156041));
#17356=CARTESIAN_POINT('Ctrl Pts',(-22.9709206878647,26.7208920000694,-52.0372587295405));
#17357=CARTESIAN_POINT('Ctrl Pts',(-23.0276747177715,26.7303614362018,-52.0337500668831));
#17358=CARTESIAN_POINT('Ctrl Pts',(-23.0354869093704,26.7316353392866,-52.0332664837724));
#17359=CARTESIAN_POINT('Ctrl Pts',(-23.0473727921776,26.7335285970121,-52.0325297728197));
#17360=CARTESIAN_POINT('Ctrl Pts',(-23.0514431483326,26.7341689469385,-52.0322773126342));
#17361=CARTESIAN_POINT('Ctrl Pts',(-23.0588218622904,26.7353152721947,-52.0318193399827));
#17362=CARTESIAN_POINT('Ctrl Pts',(-23.0621298065346,26.7358239041175,-52.0316139122222));
#17363=CARTESIAN_POINT('Ctrl Pts',(-23.0687433907608,26.7368302703849,-52.0312029686578));
#17364=CARTESIAN_POINT('Ctrl Pts',(-23.0720490248952,26.7373280161271,-52.0309974534865));
#17365=CARTESIAN_POINT('Ctrl Pts',(-23.0813489744693,26.7387135611872,-52.0304189370871));
#17366=CARTESIAN_POINT('Ctrl Pts',(-23.0873450047798,26.7395895949876,-52.0300455629974));
#17367=CARTESIAN_POINT('Ctrl Pts',(-23.111981878885,26.7431181591284,-52.0285098220641));
#17368=CARTESIAN_POINT('Ctrl Pts',(-23.1306430290408,26.7456241722117,-52.0273428214682));
#17369=CARTESIAN_POINT('Ctrl Pts',(-23.1640333561768,26.7498106347543,-52.0252477044594));
#17370=CARTESIAN_POINT('Ctrl Pts',(-23.1787543044849,26.7515532613535,-52.024321593746));
#17371=CARTESIAN_POINT('Ctrl Pts',(-23.1986194097384,26.7537659752613,-52.0230685019021));
#17372=CARTESIAN_POINT('Ctrl Pts',(-23.2037536066594,26.7543253663877,-52.0227443346885));
#17373=CARTESIAN_POINT('Ctrl Pts',(-23.2146324125687,26.7554842016428,-52.0220568155192));
#17374=CARTESIAN_POINT('Ctrl Pts',(-23.2203773270289,26.7560805481435,-52.0216933680463));
#17375=CARTESIAN_POINT('Ctrl Pts',(-23.2310744049971,26.757161891972,-52.0210159130463));
#17376=CARTESIAN_POINT('Ctrl Pts',(-23.2360261562994,26.7576508708719,-52.0207020303228));
#17377=CARTESIAN_POINT('Ctrl Pts',(-23.2478186954159,26.7587877977416,-52.0199538420098));
#17378=CARTESIAN_POINT('Ctrl Pts',(-23.2546604415329,26.7594253369291,-52.0195192165184));
#17379=CARTESIAN_POINT('Ctrl Pts',(-23.2652194806505,26.7603752143709,-52.0188476022211));
#17380=CARTESIAN_POINT('Ctrl Pts',(-23.2689353941579,26.7607029901135,-52.0186110877008));
#17381=CARTESIAN_POINT('Ctrl Pts',(-23.283166141259,26.7619333687518,-52.0177046933082));
#17382=CARTESIAN_POINT('Ctrl Pts',(-23.2936847278869,26.7627907644519,-52.0170334397426));
#17383=CARTESIAN_POINT('Ctrl Pts',(-23.3249327906844,26.7651834242278,-52.0150354407307));
#17384=CARTESIAN_POINT('Ctrl Pts',(-23.3456728233556,26.7665697954185,-52.0137042613274));
#17385=CARTESIAN_POINT('Ctrl Pts',(-23.6686483442261,26.7850226062479,-51.9928953221564));
#17386=CARTESIAN_POINT('Ctrl Pts',(-23.9717713427006,26.759616119192,-51.9720794330503));
#17387=CARTESIAN_POINT('Ctrl Pts',(-24.3322351210805,26.6774115952042,-51.9473575928224));
#17388=CARTESIAN_POINT('Ctrl Pts',(-24.3971819737005,26.6604506227334,-51.942914114474));
#17389=CARTESIAN_POINT('Ctrl Pts',(-24.5104023337608,26.6270728565242,-51.9352378830386));
#17390=CARTESIAN_POINT('Ctrl Pts',(-24.5589045377762,26.6115157998673,-51.9319727011703));
#17391=CARTESIAN_POINT('Ctrl Pts',(-24.612817154255,26.592802717127,-51.928385115289));
#17392=CARTESIAN_POINT('Ctrl Pts',(-24.6186078045001,26.5907742337236,-51.9280003267181));
#17393=CARTESIAN_POINT('Ctrl Pts',(-24.6275597757297,26.5876095980357,-51.9274063549016));
#17394=CARTESIAN_POINT('Ctrl Pts',(-24.6307251343487,26.5864850329469,-51.9271965022155));
#17395=CARTESIAN_POINT('Ctrl Pts',(-24.6359824289321,26.5846079978574,-51.9268482538467));
#17396=CARTESIAN_POINT('Ctrl Pts',(-24.6380753453527,26.5838583121055,-51.9267096941818));
#17397=CARTESIAN_POINT('Ctrl Pts',(-24.642067767234,26.582423557765,-51.9264455290876));
#17398=CARTESIAN_POINT('Ctrl Pts',(-24.6439674066093,26.5817388688468,-51.9263199010695));
#17399=CARTESIAN_POINT('Ctrl Pts',(-24.6474441788392,26.580482038943,-51.9260900933942));
#17400=CARTESIAN_POINT('Ctrl Pts',(-24.6490215000685,26.5799104548481,-51.9259858811078));
#17401=CARTESIAN_POINT('Ctrl Pts',(-24.6524001718527,26.5786831180896,-51.925762752307));
#17402=CARTESIAN_POINT('Ctrl Pts',(-24.6542013787628,26.5780269916609,-51.9256438589628));
#17403=CARTESIAN_POINT('Ctrl Pts',(-24.6594332379648,26.5761158907409,-51.9252986852145));
#17404=CARTESIAN_POINT('Ctrl Pts',(-24.6628623574923,26.5748566847423,-51.925072658772));
#17405=CARTESIAN_POINT('Ctrl Pts',(-24.6783439831259,26.5691417901984,-51.9240531270939));
#17406=CARTESIAN_POINT('Ctrl Pts',(-24.6903721346525,26.5646197923191,-51.9232635477096));
#17407=CARTESIAN_POINT('Ctrl Pts',(-24.8975101061039,26.4853287956925,-51.9097045484926));
#17408=CARTESIAN_POINT('Ctrl Pts',(-25.0849546137523,26.3918179824922,-51.8980072591855));
#17409=CARTESIAN_POINT('Ctrl Pts',(-25.3341159196798,26.235617349404,-51.8815686660606));
#17410=CARTESIAN_POINT('Ctrl Pts',(-25.4043674513326,26.187601656175,-51.8768256195252));
#17411=CARTESIAN_POINT('Ctrl Pts',(-25.5528892293528,26.0772194463773,-51.8664119769963));
#17412=CARTESIAN_POINT('Ctrl Pts',(-25.6303186225467,26.0138756113528,-51.8607297364876));
#17413=CARTESIAN_POINT('Ctrl Pts',(-25.7538376891319,25.9028468228143,-51.8510898653242));
#17414=CARTESIAN_POINT('Ctrl Pts',(-25.8016265927918,25.8571555253527,-51.8472031435511));
#17415=CARTESIAN_POINT('Ctrl Pts',(-25.8788917065523,25.7785930042181,-51.8406209434621));
#17416=CARTESIAN_POINT('Ctrl Pts',(-25.9091591729469,25.7465268389901,-51.8379605244546));
#17417=CARTESIAN_POINT('Ctrl Pts',(-25.9439092182099,25.7081645083122,-51.8348035436568));
#17418=CARTESIAN_POINT('Ctrl Pts',(-25.9490398907663,25.7024596862411,-51.8343347286017));
#17419=CARTESIAN_POINT('Ctrl Pts',(-25.95686028813,25.6937014409633,-51.8336159640884));
#17420=CARTESIAN_POINT('Ctrl Pts',(-25.9595647079522,25.6906611275184,-51.8333666331414));
#17421=CARTESIAN_POINT('Ctrl Pts',(-25.9644810015687,25.6851130982854,-51.8329119701966));
#17422=CARTESIAN_POINT('Ctrl Pts',(-25.966694747484,25.6826070428281,-51.832706717055));
#17423=CARTESIAN_POINT('Ctrl Pts',(-25.9711334454713,25.6775664573033,-51.8322941148941));
#17424=CARTESIAN_POINT('Ctrl Pts',(-25.9733583271021,25.6750318710384,-51.8320867633065));
#17425=CARTESIAN_POINT('Ctrl Pts',(-25.9796665791009,25.6678227133804,-51.8314973260264));
#17426=CARTESIAN_POINT('Ctrl Pts',(-25.9837404126964,25.6631398500943,-51.8311148440127));
#17427=CARTESIAN_POINT('Ctrl Pts',(-26.0008849845853,25.6433168431819,-51.8294974149155));
#17428=CARTESIAN_POINT('Ctrl Pts',(-26.0138279312494,25.6280672137208,-51.8282571969842));
#17429=CARTESIAN_POINT('Ctrl Pts',(-26.2733492822518,25.3164603535922,-51.8029923768085));
#17430=CARTESIAN_POINT('Ctrl Pts',(-26.4648703881453,24.9783886693485,-51.7764301520398));
#17431=CARTESIAN_POINT('Ctrl Pts',(-26.6190031122065,24.5379295180845,-51.7453319152465));
#17432=CARTESIAN_POINT('Ctrl Pts',(-26.6429590267875,24.4601452085407,-51.7399831899107));
#17433=CARTESIAN_POINT('Ctrl Pts',(-26.6722356842628,24.3504846098654,-51.7327141226101));
#17434=CARTESIAN_POINT('Ctrl Pts',(-26.680060041981,24.3193138607931,-51.7306780417303));
#17435=CARTESIAN_POINT('Ctrl Pts',(-26.688466199439,24.2835693354726,-51.7283815803464));
#17436=CARTESIAN_POINT('Ctrl Pts',(-26.6895056878486,24.2791065509039,-51.728095542567));
#17437=CARTESIAN_POINT('Ctrl Pts',(-26.6910593632357,24.2723712462426,-51.7276648919206));
#17438=CARTESIAN_POINT('Ctrl Pts',(-26.6915806042266,24.2701003848977,-51.7275198731515));
#17439=CARTESIAN_POINT('Ctrl Pts',(-26.6925151718729,24.2660084605588,-51.727258884052));
#17440=CARTESIAN_POINT('Ctrl Pts',(-26.692929377438,24.2641876077711,-51.7271428629701));
#17441=CARTESIAN_POINT('Ctrl Pts',(-26.6938157710736,24.2602752916347,-51.7268938268155));
#17442=CARTESIAN_POINT('Ctrl Pts',(-26.6942874533587,24.2581837225802,-51.7267608415514));
#17443=CARTESIAN_POINT('Ctrl Pts',(-26.6955507053046,24.2525559510441,-51.726403424794));
#17444=CARTESIAN_POINT('Ctrl Pts',(-26.6963384015977,24.2490188683528,-51.7261792174017));
#17445=CARTESIAN_POINT('Ctrl Pts',(-26.6999194962568,24.2328094633972,-51.725153682713));
#17446=CARTESIAN_POINT('Ctrl Pts',(-26.7026423576825,24.2201214376259,-51.7243563710701));
#17447=CARTESIAN_POINT('Ctrl Pts',(-26.7501016854109,23.9922699899402,-51.7101299256025));
#17448=CARTESIAN_POINT('Ctrl Pts',(-26.7727983690918,23.7730645285911,-51.6978852062535));
#17449=CARTESIAN_POINT('Ctrl Pts',(-26.77325117555,23.2821927916021,-51.6704564854239));
#17450=CARTESIAN_POINT('Ctrl Pts',(-26.7393135786712,23.0122566572046,-51.6552875631999));
#17451=CARTESIAN_POINT('Ctrl Pts',(-26.6677793148311,22.7332863647463,-51.6378359715757));
#17452=CARTESIAN_POINT('Ctrl Pts',(-26.6634234847531,22.7168417318907,-51.6368009779229));
#17453=CARTESIAN_POINT('Ctrl Pts',(-26.6574041616154,22.6948227370646,-51.6354064742231));
#17454=CARTESIAN_POINT('Ctrl Pts',(-26.6558554220354,22.6892170668814,-51.6350507001506));
#17455=CARTESIAN_POINT('Ctrl Pts',(-26.6534057783083,22.6804431619201,-51.6344926518395));
#17456=CARTESIAN_POINT('Ctrl Pts',(-26.6525151705972,22.6772720445952,-51.6342907134743));
#17457=CARTESIAN_POINT('Ctrl Pts',(-26.6507987944088,22.671196473737,-51.6339033456216));
#17458=CARTESIAN_POINT('Ctrl Pts',(-26.6499738019086,22.6682918028937,-51.6337179416275));
#17459=CARTESIAN_POINT('Ctrl Pts',(-26.6480302146227,22.6614851456829,-51.6332829873689));
#17460=CARTESIAN_POINT('Ctrl Pts',(-26.6469083295029,22.6575841112009,-51.6330333298396));
#17461=CARTESIAN_POINT('Ctrl Pts',(-26.6436575214771,22.6463602327161,-51.6323139367552));
#17462=CARTESIAN_POINT('Ctrl Pts',(-26.6415099832622,22.6390428491901,-51.6318435929266));
#17463=CARTESIAN_POINT('Ctrl Pts',(-26.6270473214732,22.590403288121,-51.6287081686714));
#17464=CARTESIAN_POINT('Ctrl Pts',(-26.6139304365051,22.5493258845263,-51.6260168919555));
#17465=CARTESIAN_POINT('Ctrl Pts',(-26.573637201482,22.4313641277324,-51.6181576116182));
#17466=CARTESIAN_POINT('Ctrl Pts',(-26.5443637019809,22.3552368254296,-51.6129218756975));
#17467=CARTESIAN_POINT('Ctrl Pts',(-26.395053584253,22.006990328839,-51.5881987289899));
#17468=CARTESIAN_POINT('Ctrl Pts',(-26.2406305830803,21.7512598188643,-51.5676242281987));
#17469=CARTESIAN_POINT('Ctrl Pts',(-25.9961280271729,21.4497600773205,-51.54193942183));
#17470=CARTESIAN_POINT('Ctrl Pts',(-25.9359235346717,21.3816232468663,-51.5360373107027));
#17471=CARTESIAN_POINT('Ctrl Pts',(-25.8684572218001,21.3114836986007,-51.5299361951867));
#17472=CARTESIAN_POINT('Ctrl Pts',(-25.863987641658,21.3068647551684,-51.5295342947188));
#17473=CARTESIAN_POINT('Ctrl Pts',(-25.8577742388518,21.3004820357207,-51.5289787992825));
#17474=CARTESIAN_POINT('Ctrl Pts',(-25.8560421921495,21.298706894716,-51.5288242930903));
#17475=CARTESIAN_POINT('Ctrl Pts',(-25.85306307765,21.2956607010867,-51.5285591354109));
#17476=CARTESIAN_POINT('Ctrl Pts',(-25.8518170059294,21.2943886829256,-51.5284484056825));
#17477=CARTESIAN_POINT('Ctrl Pts',(-25.8492422924765,21.2917647111907,-51.5282199763358));
#17478=CARTESIAN_POINT('Ctrl Pts',(-25.847913514779,21.2904128996919,-51.5281022885555));
#17479=CARTESIAN_POINT('Ctrl Pts',(-25.8447934200369,21.2872443161379,-51.5278264175924));
#17480=CARTESIAN_POINT('Ctrl Pts',(-25.8430011321461,21.2854284927928,-51.5276683112942));
#17481=CARTESIAN_POINT('Ctrl Pts',(-25.8371834296547,21.2795483781905,-51.5271562726114));
#17482=CARTESIAN_POINT('Ctrl Pts',(-25.8331493207149,21.2754926461995,-51.5268030248629));
#17483=CARTESIAN_POINT('Ctrl Pts',(-25.7258047875243,21.16814590025,-51.5174505632922));
#17484=CARTESIAN_POINT('Ctrl Pts',(-25.6155843810992,21.0719715418063,-51.5090014812559));
#17485=CARTESIAN_POINT('Ctrl Pts',(-25.2203742665292,20.7718748525581,-51.4808987789746));
#17486=CARTESIAN_POINT('Ctrl Pts',(-24.908944561337,20.607015498601,-51.4619701653074));
#17487=CARTESIAN_POINT('Ctrl Pts',(-24.5575474500855,20.4888966916738,-51.4395540331151));
#17488=CARTESIAN_POINT('Ctrl Pts',(-24.5379425440212,20.4825154111626,-51.4383013293991));
#17489=CARTESIAN_POINT('Ctrl Pts',(-24.5122869261745,20.4744360806918,-51.4366588584812));
#17490=CARTESIAN_POINT('Ctrl Pts',(-24.5062902764446,20.4725669002253,-51.436274730895));
#17491=CARTESIAN_POINT('Ctrl Pts',(-24.4970512119608,20.4697166534585,-51.4356825486539));
#17492=CARTESIAN_POINT('Ctrl Pts',(-24.4938126273699,20.4687231413165,-51.4354749029845));
#17493=CARTESIAN_POINT('Ctrl Pts',(-24.4876838619079,20.4668535655714,-51.4350818208016));
#17494=CARTESIAN_POINT('Ctrl Pts',(-24.484794002366,20.465976454128,-51.4348964189028));
#17495=CARTESIAN_POINT('Ctrl Pts',(-24.4782974285923,20.4640146249744,-51.4344795007577));
#17496=CARTESIAN_POINT('Ctrl Pts',(-24.4746900414402,20.4629321664071,-51.4342479107452));
#17497=CARTESIAN_POINT('Ctrl Pts',(-24.4672039506104,20.4607001330859,-51.4337671315724));
#17498=CARTESIAN_POINT('Ctrl Pts',(-24.4633249652806,20.4595515336705,-51.4335179109159));
#17499=CARTESIAN_POINT('Ctrl Pts',(-24.4535417070031,20.4566746555556,-51.4328890886992));
#17500=CARTESIAN_POINT('Ctrl Pts',(-24.4476346479032,20.4549559794022,-51.432509173585));
#17501=CARTESIAN_POINT('Ctrl Pts',(-24.3649360431675,20.4311512061691,-51.4271869749393));
#17502=CARTESIAN_POINT('Ctrl Pts',(-24.2873600528845,20.4119133270749,-51.422152382408));
#17503=CARTESIAN_POINT('Ctrl Pts',(-24.1383073133034,20.3807813694407,-51.4123861213722));
#17504=CARTESIAN_POINT('Ctrl Pts',(-24.0669861380849,20.368375565872,-51.4076734799077));
#17505=CARTESIAN_POINT('Ctrl Pts',(-23.8282706697898,20.3350902151898,-51.3917824677408));
#17506=CARTESIAN_POINT('Ctrl Pts',(-23.6596700038075,20.3249490776832,-51.3803517546932));
#17507=CARTESIAN_POINT('Ctrl Pts',(-23.3070572731419,20.3314260116111,-51.3564940687527));
#17508=CARTESIAN_POINT('Ctrl Pts',(-23.1236511305305,20.3505623782717,-51.3441156252281));
#17509=CARTESIAN_POINT('Ctrl Pts',(-22.9323261645463,20.3872792991368,-51.3318475428132));
#17510=CARTESIAN_POINT('Ctrl Pts',(-22.9217998279379,20.3893539455351,-51.3311747363232));
#17511=CARTESIAN_POINT('Ctrl Pts',(-22.9079472280528,20.3921561037545,-51.3302923524473));
#17512=CARTESIAN_POINT('Ctrl Pts',(-22.9046116369511,20.3928363433303,-51.3300801132109));
#17513=CARTESIAN_POINT('Ctrl Pts',(-22.8994484827568,20.3938978086633,-51.3297519537983));
#17514=CARTESIAN_POINT('Ctrl Pts',(-22.8976201753688,20.3942753367144,-51.3296358213192));
#17515=CARTESIAN_POINT('Ctrl Pts',(-22.8939636944171,20.3950336784642,-51.3294037082599));
#17516=CARTESIAN_POINT('Ctrl Pts',(-22.8921355353989,20.3954144900626,-51.3292877288838));
#17517=CARTESIAN_POINT('Ctrl Pts',(-22.8880267482298,20.3962740909557,-51.3290272262007));
#17518=CARTESIAN_POINT('Ctrl Pts',(-22.8857463126106,20.3967537640061,-51.3288827547734));
#17519=CARTESIAN_POINT('Ctrl Pts',(-22.8789813305356,20.3981843927773,-51.3284545007411));
#17520=CARTESIAN_POINT('Ctrl Pts',(-22.8744982664322,20.3991424492825,-51.3281711262704));
#17521=CARTESIAN_POINT('Ctrl Pts',(-22.8385478174045,20.4069055155296,-51.3259019889037));
#17522=CARTESIAN_POINT('Ctrl Pts',(-22.8071805313547,20.4141724530473,-51.323942369801));
#17523=CARTESIAN_POINT('Ctrl Pts',(-22.6967159199258,20.4415146134322,-51.3170960638365));
#17524=CARTESIAN_POINT('Ctrl Pts',(-22.6182723452372,20.4641236746936,-51.312333990133));
#17525=CARTESIAN_POINT('Ctrl Pts',(-22.1750010442751,20.610330876928,-51.2855623696668));
#17526=CARTESIAN_POINT('Ctrl Pts',(-21.8338395819266,20.7955446747904,-51.2650698896105));
#17527=CARTESIAN_POINT('Ctrl Pts',(-21.5178240766507,21.049102579892,-51.240561750116));
#17528=CARTESIAN_POINT('Ctrl Pts',(-21.5023620992083,21.0617467039201,-51.2393478768252));
#17529=CARTESIAN_POINT('Ctrl Pts',(-21.4822534188262,21.0785050295087,-51.2377493411908));
#17530=CARTESIAN_POINT('Ctrl Pts',(-21.4774994217515,21.0824902680724,-51.2373699500574));
#17531=CARTESIAN_POINT('Ctrl Pts',(-21.4701792119187,21.0886628184276,-51.2367834714108));
#17532=CARTESIAN_POINT('Ctrl Pts',(-21.4676048577017,21.0908404885469,-51.236576780247));
#17533=CARTESIAN_POINT('Ctrl Pts',(-21.4625353397269,21.0951425081735,-51.2361688853135));
#17534=CARTESIAN_POINT('Ctrl Pts',(-21.4600399886969,21.0972666315719,-51.2359676910047));
#17535=CARTESIAN_POINT('Ctrl Pts',(-21.4545368872986,21.1019655435187,-51.235523062998));
#17536=CARTESIAN_POINT('Ctrl Pts',(-21.4515306367522,21.1045420733403,-51.2352795574505));
#17537=CARTESIAN_POINT('Ctrl Pts',(-21.4453094796805,21.109893880163,-51.234774369141));
#17538=CARTESIAN_POINT('Ctrl Pts',(-21.4420952975684,21.1126699841176,-51.2345126522897));
#17539=CARTESIAN_POINT('Ctrl Pts',(-21.4338775382209,21.1197961119896,-51.2338416898385));
#17540=CARTESIAN_POINT('Ctrl Pts',(-21.4288818982841,21.1241552220767,-51.2334320658743));
#17541=CARTESIAN_POINT('Ctrl Pts',(-21.3222126570088,21.2178143441682,-51.2246480449216));
#17542=CARTESIAN_POINT('Ctrl Pts',(-21.2262640280818,21.3134024529221,-51.2160055639916));
#17543=CARTESIAN_POINT('Ctrl Pts',(-20.9027265161788,21.6790743524155,-51.1839878552845));
#17544=CARTESIAN_POINT('Ctrl Pts',(-20.7138886881856,21.9799995816138,-51.1592019920556));
#17545=CARTESIAN_POINT('Ctrl Pts',(-20.5680105986171,22.3283829022343,-51.1351328512517));
#17546=CARTESIAN_POINT('Ctrl Pts',(-20.5586979092823,22.3513641417916,-51.1335664065855));
#17547=CARTESIAN_POINT('Ctrl Pts',(-20.5481370860205,22.3783149768094,-51.1317560411249));
#17548=CARTESIAN_POINT('Ctrl Pts',(-20.5466305816187,22.3821814879705,-51.1314969529947));
#17549=CARTESIAN_POINT('Ctrl Pts',(-20.5442392615321,22.3883541355109,-51.1310843619695));
#17550=CARTESIAN_POINT('Ctrl Pts',(-20.5433496282864,22.3906583815624,-51.1309305699409));
#17551=CARTESIAN_POINT('Ctrl Pts',(-20.5417841498454,22.3947270547631,-51.1306594200765));
#17552=CARTESIAN_POINT('Ctrl Pts',(-20.5411072066387,22.3964910549615,-51.1305419955694));
#17553=CARTESIAN_POINT('Ctrl Pts',(-20.5397017037959,22.4001632104066,-51.1302978311048));
#17554=CARTESIAN_POINT('Ctrl Pts',(-20.5389734081932,22.4020714594231,-51.1301711073665));
#17555=CARTESIAN_POINT('Ctrl Pts',(-20.5370860831278,22.40703069515,-51.1298421776322));
#17556=CARTESIAN_POINT('Ctrl Pts',(-20.5359298696236,22.4100827621117,-51.1296401421094));
#17557=CARTESIAN_POINT('Ctrl Pts',(-20.5310128279783,22.4231220767256,-51.12877866488));
#17558=CARTESIAN_POINT('Ctrl Pts',(-20.5272969273411,22.4331263648332,-51.1281219018149));
#17559=CARTESIAN_POINT('Ctrl Pts',(-20.4684252477398,22.5940709547398,-51.1176206487024));
#17560=CARTESIAN_POINT('Ctrl Pts',(-20.4245769699635,22.7489346392783,-51.1084199970133));
#17561=CARTESIAN_POINT('Ctrl Pts',(-20.3525187137542,23.1023701891515,-51.0881096158864));
#17562=CARTESIAN_POINT('Ctrl Pts',(-20.3308950044511,23.3015828607029,-51.077106659923));
#17563=CARTESIAN_POINT('Ctrl Pts',(-20.3257385774263,23.6425092801541,-51.0575808891623));
#17564=CARTESIAN_POINT('Ctrl Pts',(-20.3328620788933,23.7834740185373,-51.0493118804113));
#17565=CARTESIAN_POINT('Ctrl Pts',(-20.3504706059953,23.934485994549,-51.0400635701361));
#17566=CARTESIAN_POINT('Ctrl Pts',(-20.3518071796368,23.9454576064803,-51.0393894681638));
#17567=CARTESIAN_POINT('Ctrl Pts',(-20.3537507391579,23.9607558053156,-51.0384464327214));
#17568=CARTESIAN_POINT('Ctrl Pts',(-20.3543101342112,23.9650884498677,-51.0381790051741));
#17569=CARTESIAN_POINT('Ctrl Pts',(-20.3552915346554,23.9725698086195,-51.0377166209411));
#17570=CARTESIAN_POINT('Ctrl Pts',(-20.355709390599,23.9757190692285,-51.0375217958141));
#17571=CARTESIAN_POINT('Ctrl Pts',(-20.3565749810297,23.982169611503,-51.0371223586216));
#17572=CARTESIAN_POINT('Ctrl Pts',(-20.3570231791587,23.985470825685,-51.0369177321179));
#17573=CARTESIAN_POINT('Ctrl Pts',(-20.3580764422194,23.9931394434956,-51.0364419113638));
#17574=CARTESIAN_POINT('Ctrl Pts',(-20.3586853515575,23.9975063044286,-51.0361705955634));
#17575=CARTESIAN_POINT('Ctrl Pts',(-20.3599864640104,24.0066994088877,-51.0355986548238));
#17576=CARTESIAN_POINT('Ctrl Pts',(-20.3606806612871,24.0115253548728,-51.0352979671656));
#17577=CARTESIAN_POINT('Ctrl Pts',(-20.3625616564966,24.0243944380355,-51.0344949417278));
#17578=CARTESIAN_POINT('Ctrl Pts',(-20.3637679382625,24.0324346518951,-51.0339919861131));
#17579=CARTESIAN_POINT('Ctrl Pts',(-20.3917246614464,24.2140868194161,-51.0226001475537));
#17580=CARTESIAN_POINT('Ctrl Pts',(-20.4325895427568,24.3851975183107,-51.0112534193078));
#17581=CARTESIAN_POINT('Ctrl Pts',(-20.5861665038666,24.8547452705939,-50.9784029695819));
#17582=CARTESIAN_POINT('Ctrl Pts',(-20.7294484550355,25.1410279188329,-50.9561787758156));
#17583=CARTESIAN_POINT('Ctrl Pts',(-20.9217725394888,25.4150523901588,-50.9349888361478));
#17584=CARTESIAN_POINT('Ctrl Pts',(-20.9312796977172,25.4283810958436,-50.933958896492));
#17585=CARTESIAN_POINT('Ctrl Pts',(-20.943000574052,25.4445512795666,-50.9327108913504));
#17586=CARTESIAN_POINT('Ctrl Pts',(-20.94511779121,25.4474619300092,-50.932486308949));
#17587=CARTESIAN_POINT('Ctrl Pts',(-20.9486132370446,25.4522504204135,-50.9321169417382));
#17588=CARTESIAN_POINT('Ctrl Pts',(-20.9499886256495,25.4541303132627,-50.9319719607284));
#17589=CARTESIAN_POINT('Ctrl Pts',(-20.9524702875869,25.4575145644505,-50.9317110123444));
#17590=CARTESIAN_POINT('Ctrl Pts',(-20.9535758277237,25.4590194489759,-50.9315949942891));
#17591=CARTESIAN_POINT('Ctrl Pts',(-20.9559538384064,25.4622505577044,-50.9313459344992));
#17592=CARTESIAN_POINT('Ctrl Pts',(-20.9572267206693,25.4639764681293,-50.9312129226274));
#17593=CARTESIAN_POINT('Ctrl Pts',(-20.9607122858286,25.4686927094224,-50.9308495160471));
#17594=CARTESIAN_POINT('Ctrl Pts',(-20.9629284337504,25.4716804936564,-50.9306193639441));
#17595=CARTESIAN_POINT('Ctrl Pts',(-20.9743923525576,25.4870802154808,-50.9294334281529));
#17596=CARTESIAN_POINT('Ctrl Pts',(-20.9837244865469,25.4994295260389,-50.928483482292));
#17597=CARTESIAN_POINT('Ctrl Pts',(-21.0406759791349,25.573675826263,-50.9227755513642));
#17598=CARTESIAN_POINT('Ctrl Pts',(-21.0904475099349,25.6338978377655,-50.9181596634146));
#17599=CARTESIAN_POINT('Ctrl Pts',(-21.1774997288823,25.7317557951212,-50.9105693189738));
#17600=CARTESIAN_POINT('Ctrl Pts',(-21.2136049266329,25.7703855749308,-50.9075477171387));
#17601=CARTESIAN_POINT('Ctrl Pts',(-21.2766902698847,25.8346373928394,-50.9024437090867));
#17602=CARTESIAN_POINT('Ctrl Pts',(-21.3031925922703,25.8607116341073,-50.9003491874576));
#17603=CARTESIAN_POINT('Ctrl Pts',(-21.3534595798391,25.908483480218,-50.8964552259784));
#17604=CARTESIAN_POINT('Ctrl Pts',(-21.3771093710663,25.9302948234613,-50.8946542630287));
#17605=CARTESIAN_POINT('Ctrl Pts',(-21.5477037864088,26.0829648691416,-50.8818523335301));
#17606=CARTESIAN_POINT('Ctrl Pts',(-21.7060229119617,26.2004683146711,-50.8709206884809));
#17607=CARTESIAN_POINT('Ctrl Pts',(-21.9396995371645,26.3427679374918,-50.8550034730067));
#17608=CARTESIAN_POINT('Ctrl Pts',(-22.0067333528666,26.3803705550361,-50.850464096738));
#17609=CARTESIAN_POINT('Ctrl Pts',(-22.0750360284016,26.415536781278,-50.8458393738826));
#17610=CARTESIAN_POINT('Origin',(-23.5502525316942,23.5502525316942,-77.3107734492734));
#17611=CARTESIAN_POINT('',(-22.0750360150599,26.4155367744089,-49.3491334787091));
#17612=CARTESIAN_POINT('',(-22.0750360207194,26.4155367773228,-49.5934531403533));
#17613=CARTESIAN_POINT('',(-22.0750360153461,26.4155367745563,-77.3107734492734));
#17614=CARTESIAN_POINT('Ctrl Pts',(-22.0750360150599,26.4155367744089,-49.3491334787091));
#17615=CARTESIAN_POINT('Ctrl Pts',(-22.0691259159558,26.412493908475,-49.3495623158237));
#17616=CARTESIAN_POINT('Ctrl Pts',(-22.0632250938881,26.4094326859608,-49.3499902916244));
#17617=CARTESIAN_POINT('Ctrl Pts',(-22.0356084854432,26.3949971452919,-49.351992246194));
#17618=CARTESIAN_POINT('Ctrl Pts',(-22.0140128525966,26.3833932332581,-49.3535547529389));
#17619=CARTESIAN_POINT('Ctrl Pts',(-21.9844229622205,26.3670559551105,-49.3556893679477));
#17620=CARTESIAN_POINT('Ctrl Pts',(-21.9763142381812,26.3625331044573,-49.3562736714923));
#17621=CARTESIAN_POINT('Ctrl Pts',(-21.9624531224613,26.3547229791749,-49.3572712021989));
#17622=CARTESIAN_POINT('Ctrl Pts',(-21.9566911673401,26.3514529234272,-49.3576854858052));
#17623=CARTESIAN_POINT('Ctrl Pts',(-21.9485948326466,26.3468249820133,-49.3582670276047));
#17624=CARTESIAN_POINT('Ctrl Pts',(-21.9462520637019,26.3454819236423,-49.3584352345438));
#17625=CARTESIAN_POINT('Ctrl Pts',(-21.9423936544358,26.3432635335765,-49.3587121446412));
#17626=CARTESIAN_POINT('Ctrl Pts',(-21.9408770400775,26.3423899124177,-49.3588209590127));
#17627=CARTESIAN_POINT('Ctrl Pts',(-21.9377093778048,26.3405617934692,-49.3590481693375));
#17628=CARTESIAN_POINT('Ctrl Pts',(-21.9360584649653,26.3396070653584,-49.3591665497985));
#17629=CARTESIAN_POINT('Ctrl Pts',(-21.9324212021028,26.337499314187,-49.3594272856177));
#17630=CARTESIAN_POINT('Ctrl Pts',(-21.9304352317322,26.3363456299852,-49.3595695978266));
#17631=CARTESIAN_POINT('Ctrl Pts',(-21.923506627991,26.3323107729891,-49.3600659198906));
#17632=CARTESIAN_POINT('Ctrl Pts',(-21.9185703970297,26.32941854073,-49.3604192127122));
#17633=CARTESIAN_POINT('Ctrl Pts',(-21.8689354191354,26.3001586310397,-49.3639688206033));
#17634=CARTESIAN_POINT('Ctrl Pts',(-21.8248689323501,26.2727262191741,-49.3670970123069));
#17635=CARTESIAN_POINT('Ctrl Pts',(-21.778063033863,26.2419952139568,-49.3704159454854));
#17636=CARTESIAN_POINT('Ctrl Pts',(-21.7746490484246,26.2397444082848,-49.3706580039756));
#17637=CARTESIAN_POINT('Ctrl Pts',(-21.5389753898331,26.0837228416099,-49.3873669026408));
#17638=CARTESIAN_POINT('Ctrl Pts',(-21.3276013259104,25.9004796844223,-49.4023852707713));
#17639=CARTESIAN_POINT('Ctrl Pts',(-21.0590572699968,25.5986155227901,-49.4252893958585));
#17640=CARTESIAN_POINT('Ctrl Pts',(-20.981250299577,25.5001416371026,-49.4325201041075));
#17641=CARTESIAN_POINT('Ctrl Pts',(-20.8788210679617,25.353697762684,-49.4431469877096));
#17642=CARTESIAN_POINT('Ctrl Pts',(-20.8493499999454,25.3092538869737,-49.4463558825097));
#17643=CARTESIAN_POINT('Ctrl Pts',(-20.8167105517051,25.2572764774925,-49.4500981094948));
#17644=CARTESIAN_POINT('Ctrl Pts',(-20.8124505142066,25.250435645089,-49.4505904184373));
#17645=CARTESIAN_POINT('Ctrl Pts',(-20.8060355151092,25.2400477126223,-49.4513377065188));
#17646=CARTESIAN_POINT('Ctrl Pts',(-20.8038616514365,25.2365122744931,-49.451591988131));
#17647=CARTESIAN_POINT('Ctrl Pts',(-20.7999620691484,25.2301426901958,-49.4520500243231));
#17648=CARTESIAN_POINT('Ctrl Pts',(-20.798233883955,25.2273100546687,-49.4522536878041));
#17649=CARTESIAN_POINT('Ctrl Pts',(-20.7945335911162,25.2212238534026,-49.4526912150723));
#17650=CARTESIAN_POINT('Ctrl Pts',(-20.7925628656177,25.2179694569693,-49.4529251291864));
#17651=CARTESIAN_POINT('Ctrl Pts',(-20.7872596075099,25.2091767139723,-49.4535570181752));
#17652=CARTESIAN_POINT('Ctrl Pts',(-20.7839379793887,25.2036318403731,-49.4539553914731));
#17653=CARTESIAN_POINT('Ctrl Pts',(-20.7692837035791,25.1790013247308,-49.4557245354168));
#17654=CARTESIAN_POINT('Ctrl Pts',(-20.7581319476875,25.1598092590007,-49.4571018780437));
#17655=CARTESIAN_POINT('Ctrl Pts',(-20.740927583315,25.1294838088069,-49.4592768128805));
#17656=CARTESIAN_POINT('Ctrl Pts',(-20.7347407287,25.1184270666214,-49.4600695080851));
#17657=CARTESIAN_POINT('Ctrl Pts',(-20.7259364637163,25.1024726011364,-49.4612129744289));
#17658=CARTESIAN_POINT('Ctrl Pts',(-20.7232662058473,25.0976040459501,-49.4615618583171));
#17659=CARTESIAN_POINT('Ctrl Pts',(-20.7172802257783,25.0866228758949,-49.4623486734307));
#17660=CARTESIAN_POINT('Ctrl Pts',(-20.7139716866925,25.080506395497,-49.4627868557418));
#17661=CARTESIAN_POINT('Ctrl Pts',(-20.709806592617,25.0727464935172,-49.4633426877643));
#17662=CARTESIAN_POINT('Ctrl Pts',(-20.708931604492,25.0711129412083,-49.463459692335));
#17663=CARTESIAN_POINT('Ctrl Pts',(-20.7047821567747,25.0633500825722,-49.4640156916099));
#17664=CARTESIAN_POINT('Ctrl Pts',(-20.7015261378426,25.0572109865896,-49.4644553268903));
#17665=CARTESIAN_POINT('Ctrl Pts',(-20.6960291968827,25.0467652400348,-49.4652032674357));
#17666=CARTESIAN_POINT('Ctrl Pts',(-20.6937780938749,25.0424639499864,-49.4655112202199));
#17667=CARTESIAN_POINT('Ctrl Pts',(-20.6896841454133,25.0345982364084,-49.4660743168653));
#17668=CARTESIAN_POINT('Ctrl Pts',(-20.687838218511,25.0310354202859,-49.4663293547703));
#17669=CARTESIAN_POINT('Ctrl Pts',(-20.6839786244681,25.0235518490328,-49.4668650128491));
#17670=CARTESIAN_POINT('Ctrl Pts',(-20.6819663384318,25.0196303942432,-49.4671456791547));
#17671=CARTESIAN_POINT('Ctrl Pts',(-20.6706729617978,24.9975107588224,-49.4687286986706));
#17672=CARTESIAN_POINT('Ctrl Pts',(-20.6615571851455,24.9792291026326,-49.4700365702729));
#17673=CARTESIAN_POINT('Ctrl Pts',(-20.5205315224112,24.6895379978154,-49.4907539376423));
#17674=CARTESIAN_POINT('Ctrl Pts',(-20.4272256431046,24.4010296392564,-49.5114947818016));
#17675=CARTESIAN_POINT('Ctrl Pts',(-20.360349998304,24.0175019709703,-49.5375402399015));
#17676=CARTESIAN_POINT('Ctrl Pts',(-20.3488211924274,23.9305683473128,-49.5433312635735));
#17677=CARTESIAN_POINT('Ctrl Pts',(-20.3385161720901,23.8176966828114,-49.5506207813762));
#17678=CARTESIAN_POINT('Ctrl Pts',(-20.3364872747463,23.7920991476344,-49.5522587060306));
#17679=CARTESIAN_POINT('Ctrl Pts',(-20.3341199585045,23.7568949923583,-49.554487959778));
#17680=CARTESIAN_POINT('Ctrl Pts',(-20.333518309329,23.7473078106942,-49.5550926754608));
#17681=CARTESIAN_POINT('Ctrl Pts',(-20.332688810562,23.7330719013884,-49.5559869380209));
#17682=CARTESIAN_POINT('Ctrl Pts',(-20.3324281570223,23.7284252453407,-49.5562782480867));
#17683=CARTESIAN_POINT('Ctrl Pts',(-20.3320287756304,23.7210186137934,-49.5567416447074));
#17684=CARTESIAN_POINT('Ctrl Pts',(-20.3318835317959,23.718259018232,-49.5569140905009));
#17685=CARTESIAN_POINT('Ctrl Pts',(-20.3316143492816,23.7130161490807,-49.5572413142629));
#17686=CARTESIAN_POINT('Ctrl Pts',(-20.331489734678,23.7105329143801,-49.5573961299677));
#17687=CARTESIAN_POINT('Ctrl Pts',(-20.3312769728162,23.7061928072554,-49.557666409968));
#17688=CARTESIAN_POINT('Ctrl Pts',(-20.3311875583144,23.70433600072,-49.5577819461307));
#17689=CARTESIAN_POINT('Ctrl Pts',(-20.3310157728409,23.7007032336661,-49.5580077982845));
#17690=CARTESIAN_POINT('Ctrl Pts',(-20.3309332650555,23.6989272866583,-49.5581181218911));
#17691=CARTESIAN_POINT('Ctrl Pts',(-20.3307396446026,23.694683943484,-49.5583815131137));
#17692=CARTESIAN_POINT('Ctrl Pts',(-20.330629898545,23.6922164815876,-49.5585345032649));
#17693=CARTESIAN_POINT('Ctrl Pts',(-20.3302474336868,23.6833887713138,-49.5590812505616));
#17694=CARTESIAN_POINT('Ctrl Pts',(-20.329990721671,23.6770277896843,-49.5594741104517));
#17695=CARTESIAN_POINT('Ctrl Pts',(-20.326499272205,23.5836477907786,-49.565225600634));
#17696=CARTESIAN_POINT('Ctrl Pts',(-20.3267735471633,23.4965240630276,-49.570391329925));
#17697=CARTESIAN_POINT('Ctrl Pts',(-20.3324562768539,23.36652413677,-49.5779407758143));
#17698=CARTESIAN_POINT('Ctrl Pts',(-20.3351960448085,23.323579019144,-49.5804087560653));
#17699=CARTESIAN_POINT('Ctrl Pts',(-20.3564168650059,23.0707531555806,-49.5948492969427));
#17700=CARTESIAN_POINT('Ctrl Pts',(-20.3945835070007,22.8630377654017,-49.6063854087763));
#17701=CARTESIAN_POINT('Ctrl Pts',(-20.4815895007542,22.5601335951613,-49.6242894523401));
#17702=CARTESIAN_POINT('Ctrl Pts',(-20.5152885023191,22.4612076004466,-49.6303124967231));
#17703=CARTESIAN_POINT('Ctrl Pts',(-20.5780311409963,22.302703984273,-49.6403883408207));
#17704=CARTESIAN_POINT('Ctrl Pts',(-20.6042130674933,22.2420752151218,-49.6443478812584));
#17705=CARTESIAN_POINT('Ctrl Pts',(-20.6358315936319,22.174629085286,-49.6488882532704));
#17706=CARTESIAN_POINT('Ctrl Pts',(-20.6394561971918,22.1669759984534,-49.6494054449437));
#17707=CARTESIAN_POINT('Ctrl Pts',(-20.6449385287891,22.1555174173792,-49.6501828435674));
#17708=CARTESIAN_POINT('Ctrl Pts',(-20.6467736835842,22.151701112229,-49.6504422645194));
#17709=CARTESIAN_POINT('Ctrl Pts',(-20.6499398124872,22.1451500643923,-49.6508884607435));
#17710=CARTESIAN_POINT('Ctrl Pts',(-20.6512671492896,22.1424135617437,-49.651075108912));
#17711=CARTESIAN_POINT('Ctrl Pts',(-20.6540059009508,22.1367875133794,-49.651459387439));
#17712=CARTESIAN_POINT('Ctrl Pts',(-20.6554177707774,22.1338981936299,-49.6516570335606));
#17713=CARTESIAN_POINT('Ctrl Pts',(-20.6588225695653,22.1269568042779,-49.6521325782717));
#17714=CARTESIAN_POINT('Ctrl Pts',(-20.6608196912004,22.1229068084962,-49.6524106234732));
#17715=CARTESIAN_POINT('Ctrl Pts',(-20.6669600030131,22.1105204672533,-49.6532627890281));
#17716=CARTESIAN_POINT('Ctrl Pts',(-20.6711307795822,22.1021979205268,-49.6538378767057));
#17717=CARTESIAN_POINT('Ctrl Pts',(-20.7192343972942,22.0072393134792,-49.6604284871116));
#17718=CARTESIAN_POINT('Ctrl Pts',(-20.7670222776059,21.922622495287,-49.6665801843234));
#17719=CARTESIAN_POINT('Ctrl Pts',(-20.8906306081776,21.7251546950487,-49.6816438569462));
#17720=CARTESIAN_POINT('Ctrl Pts',(-20.9699079564834,21.6146942467331,-49.6906677397866));
#17721=CARTESIAN_POINT('Ctrl Pts',(-21.1787037325698,21.3594808978904,-49.7128666434198));
#17722=CARTESIAN_POINT('Ctrl Pts',(-21.3147957074456,21.220776250317,-49.7261356604317));
#17723=CARTESIAN_POINT('Ctrl Pts',(-21.5196051820531,21.046614907131,-49.7438540995113));
#17724=CARTESIAN_POINT('Ctrl Pts',(-21.578357124272,21.000083796899,-49.748709720288));
#17725=CARTESIAN_POINT('Ctrl Pts',(-21.6448726637571,20.9510787720001,-49.7539157078703));
#17726=CARTESIAN_POINT('Ctrl Pts',(-21.6510789261483,20.9465405097836,-49.7543987423098));
#17727=CARTESIAN_POINT('Ctrl Pts',(-21.6605017494822,20.9397017889718,-49.7551279502848));
#17728=CARTESIAN_POINT('Ctrl Pts',(-21.6637063477573,20.9373850081739,-49.7553752190289));
#17729=CARTESIAN_POINT('Ctrl Pts',(-21.6689218576993,20.9336290256352,-49.7557764601246));
#17730=CARTESIAN_POINT('Ctrl Pts',(-21.6709301639283,20.9321862385135,-49.7559306775886));
#17731=CARTESIAN_POINT('Ctrl Pts',(-21.6747885974224,20.9294210290101,-49.756226413994));
#17732=CARTESIAN_POINT('Ctrl Pts',(-21.6766384664507,20.9280982515625,-49.7563679574608));
#17733=CARTESIAN_POINT('Ctrl Pts',(-21.6799806553775,20.9257137102094,-49.7566232456918));
#17734=CARTESIAN_POINT('Ctrl Pts',(-21.6814724770791,20.9246512625842,-49.7567370379822));
#17735=CARTESIAN_POINT('Ctrl Pts',(-21.6844808404255,20.9225126251233,-49.7569661888592));
#17736=CARTESIAN_POINT('Ctrl Pts',(-21.685997402147,20.9214364802132,-49.7570815443175));
#17737=CARTESIAN_POINT('Ctrl Pts',(-21.6902636479221,20.9184147211751,-49.7574055958832));
#17738=CARTESIAN_POINT('Ctrl Pts',(-21.6930154623841,20.9164720971741,-49.7576140845964));
#17739=CARTESIAN_POINT('Ctrl Pts',(-21.7043152333803,20.9085216190895,-49.7584680480524));
#17740=CARTESIAN_POINT('Ctrl Pts',(-21.7128894594236,20.9025509488741,-49.7591109872184));
#17741=CARTESIAN_POINT('Ctrl Pts',(-21.8607810069994,20.8006309130596,-49.7701170341141));
#17742=CARTESIAN_POINT('Ctrl Pts',(-22.0074337458379,20.7157400745456,-49.7797662405502));
#17743=CARTESIAN_POINT('Ctrl Pts',(-22.3525485525572,20.5507311621223,-49.801266138834));
#17744=CARTESIAN_POINT('Ctrl Pts',(-22.5536536195101,20.478052816462,-49.813007878494));
#17745=CARTESIAN_POINT('Ctrl Pts',(-22.8404728745875,20.4055520668102,-49.8300824343979));
#17746=CARTESIAN_POINT('Ctrl Pts',(-22.9212246442353,20.3884096405883,-49.8349186477814));
#17747=CARTESIAN_POINT('Ctrl Pts',(-23.0442790305731,20.3671876139351,-49.8423842776353));
#17748=CARTESIAN_POINT('Ctrl Pts',(-23.0861534703752,20.3608131992344,-49.8449411316729));
#17749=CARTESIAN_POINT('Ctrl Pts',(-23.1356628229357,20.3542721628591,-49.8479872100228));
#17750=CARTESIAN_POINT('Ctrl Pts',(-23.1431891727396,20.3533048366527,-49.848450893938));
#17751=CARTESIAN_POINT('Ctrl Pts',(-23.1547385284602,20.3518618979489,-49.8491634057405));
#17752=CARTESIAN_POINT('Ctrl Pts',(-23.1587591672811,20.3513672698933,-49.8494116317708));
#17753=CARTESIAN_POINT('Ctrl Pts',(-23.1660992764346,20.3504783188219,-49.849865130603));
#17754=CARTESIAN_POINT('Ctrl Pts',(-23.169418452664,20.3500815767288,-49.8500703266021));
#17755=CARTESIAN_POINT('Ctrl Pts',(-23.1760983761141,20.3492936631634,-49.8504835426966));
#17756=CARTESIAN_POINT('Ctrl Pts',(-23.1794591337816,20.3489026185968,-49.8506915665279));
#17757=CARTESIAN_POINT('Ctrl Pts',(-23.1890410559834,20.3478029946427,-49.8512850394249));
#17758=CARTESIAN_POINT('Ctrl Pts',(-23.1952636529138,20.3471072551569,-49.8516708936641));
#17759=CARTESIAN_POINT('Ctrl Pts',(-23.2218212977175,20.3442162216857,-49.8533196316222));
#17760=CARTESIAN_POINT('Ctrl Pts',(-23.2421746142569,20.3421964439256,-49.8545880422652));
#17761=CARTESIAN_POINT('Ctrl Pts',(-23.623560302085,20.3080122024984,-49.8784504722928));
#17762=CARTESIAN_POINT('Ctrl Pts',(-23.9873870202627,20.3368021084894,-49.9032415357527));
#17763=CARTESIAN_POINT('Ctrl Pts',(-24.4665956615241,20.4577054378386,-49.9363884148461));
#17764=CARTESIAN_POINT('Ctrl Pts',(-24.5924652140133,20.4978216552833,-49.9450929520787));
#17765=CARTESIAN_POINT('Ctrl Pts',(-24.7200889308477,20.5473165969402,-49.9536806207586));
#17766=CARTESIAN_POINT('Ctrl Pts',(-24.7246397445941,20.5490934049673,-49.9539865129444));
#17767=CARTESIAN_POINT('Ctrl Pts',(-24.731846715071,20.5519261788487,-49.9544704045179));
#17768=CARTESIAN_POINT('Ctrl Pts',(-24.7345055146659,20.5529753331637,-49.9546488054395));
#17769=CARTESIAN_POINT('Ctrl Pts',(-24.7395417216747,20.554970352711,-49.9549865003513));
#17770=CARTESIAN_POINT('Ctrl Pts',(-24.7419194030628,20.5559155137667,-49.9551458364193));
#17771=CARTESIAN_POINT('Ctrl Pts',(-24.7460330501115,20.5575564208503,-49.9554213363765));
#17772=CARTESIAN_POINT('Ctrl Pts',(-24.7477695380206,20.5582508472503,-49.9555375806456));
#17773=CARTESIAN_POINT('Ctrl Pts',(-24.7511395163107,20.5596019148371,-49.9557630718101));
#17774=CARTESIAN_POINT('Ctrl Pts',(-24.7527730702585,20.5602583818175,-49.9558723291145));
#17775=CARTESIAN_POINT('Ctrl Pts',(-24.7566356988388,20.561814311769,-49.9561305655069));
#17776=CARTESIAN_POINT('Ctrl Pts',(-24.7588643105157,20.5627149321883,-49.9562794739778));
#17777=CARTESIAN_POINT('Ctrl Pts',(-24.7654905943,20.5654013558052,-49.9567219716669));
#17778=CARTESIAN_POINT('Ctrl Pts',(-24.7698853558342,20.5671943918027,-49.9570151240182));
#17779=CARTESIAN_POINT('Ctrl Pts',(-24.8099544235803,20.5836456782026,-49.9596850907256));
#17780=CARTESIAN_POINT('Ctrl Pts',(-24.845368789658,20.5989343038941,-49.9620243426277));
#17781=CARTESIAN_POINT('Ctrl Pts',(-25.0133085586637,20.6750404726049,-49.9730578589526));
#17782=CARTESIAN_POINT('Ctrl Pts',(-25.1418932780101,20.7441758041256,-49.9813305777251));
#17783=CARTESIAN_POINT('Ctrl Pts',(-25.3440782575088,20.8712693727745,-49.99473253995));
#17784=CARTESIAN_POINT('Ctrl Pts',(-25.420613634216,20.9241316253425,-49.999906843828));
#17785=CARTESIAN_POINT('Ctrl Pts',(-25.5770310612405,21.0424785320367,-50.0108964125547));
#17786=CARTESIAN_POINT('Ctrl Pts',(-25.6562653236546,21.1086403413865,-50.0167139084268));
#17787=CARTESIAN_POINT('Ctrl Pts',(-25.8275432788986,21.266209454202,-50.0301014258739));
#17788=CARTESIAN_POINT('Ctrl Pts',(-25.9175114863494,21.3595940509773,-50.037729175639));
#17789=CARTESIAN_POINT('Ctrl Pts',(-26.0083381314482,21.4660164117986,-50.0462453674974));
#17790=CARTESIAN_POINT('Ctrl Pts',(-26.0150293952991,21.4739336669997,-50.0468778893076));
#17791=CARTESIAN_POINT('Ctrl Pts',(-26.0246346015815,21.4854106261046,-50.0477933672426));
#17792=CARTESIAN_POINT('Ctrl Pts',(-26.0275793504165,21.4889445596168,-50.0480750622075));
#17793=CARTESIAN_POINT('Ctrl Pts',(-26.0326927827819,21.4951078703413,-50.0485660156373));
#17794=CARTESIAN_POINT('Ctrl Pts',(-26.0348648853371,21.4977344120937,-50.048775134348));
#17795=CARTESIAN_POINT('Ctrl Pts',(-26.0390446612811,21.5028050226104,-50.0491786443299));
#17796=CARTESIAN_POINT('Ctrl Pts',(-26.0410529122718,21.5052486122011,-50.0493730118053));
#17797=CARTESIAN_POINT('Ctrl Pts',(-26.0457926434958,21.5110331379632,-50.0498329155719));
#17798=CARTESIAN_POINT('Ctrl Pts',(-26.0485210122141,21.5143766061185,-50.0500985775737));
#17799=CARTESIAN_POINT('Ctrl Pts',(-26.056609808026,21.5243297326302,-50.0508889457516));
#17800=CARTESIAN_POINT('Ctrl Pts',(-26.0619507473045,21.5309551152992,-50.0514144372414));
#17801=CARTESIAN_POINT('Ctrl Pts',(-26.1106123824566,21.5918111497292,-50.0562356908908));
#17802=CARTESIAN_POINT('Ctrl Pts',(-26.1521938400078,21.647403239183,-50.0606004305876));
#17803=CARTESIAN_POINT('Ctrl Pts',(-26.1977801256834,21.7126402357766,-50.0656841701246));
#17804=CARTESIAN_POINT('Ctrl Pts',(-26.20357473441,21.7210170094307,-50.0663362337197));
#17805=CARTESIAN_POINT('Ctrl Pts',(-26.3559778343107,21.9435810257917,-50.0836422213472));
#17806=CARTESIAN_POINT('Ctrl Pts',(-26.4761966022829,22.1746451062456,-50.1012653627369));
#17807=CARTESIAN_POINT('Ctrl Pts',(-26.5969500618658,22.4962962127341,-50.1244673141327));
#17808=CARTESIAN_POINT('Ctrl Pts',(-26.6234155195122,22.5761579045349,-50.1301168416261));
#17809=CARTESIAN_POINT('Ctrl Pts',(-26.6639125476698,22.7165363219465,-50.1397670341973));
#17810=CARTESIAN_POINT('Ctrl Pts',(-26.6793761391667,22.7765937253411,-50.1438086556587));
#17811=CARTESIAN_POINT('Ctrl Pts',(-26.6992497716561,22.86417190174,-50.1495422905182));
#17812=CARTESIAN_POINT('Ctrl Pts',(-26.7050505240801,22.891359518013,-50.1513001436345));
#17813=CARTESIAN_POINT('Ctrl Pts',(-26.7113653586342,22.9229545184331,-50.1533147485235));
#17814=CARTESIAN_POINT('Ctrl Pts',(-26.7122228002378,22.9272909570457,-50.1535906406513));
#17815=CARTESIAN_POINT('Ctrl Pts',(-26.7135120748713,22.9338825963787,-50.1540090658486));
#17816=CARTESIAN_POINT('Ctrl Pts',(-26.7139504199097,22.9361364947424,-50.1541519711122));
#17817=CARTESIAN_POINT('Ctrl Pts',(-26.7147404418734,22.9402219528891,-50.1544106969069));
#17818=CARTESIAN_POINT('Ctrl Pts',(-26.7150929365947,22.9420533436724,-50.1545265641887));
#17819=CARTESIAN_POINT('Ctrl Pts',(-26.7157986723795,22.9457372298634,-50.1547594088259));
#17820=CARTESIAN_POINT('Ctrl Pts',(-26.7161518757414,22.9475897218564,-50.1548763836876));
#17821=CARTESIAN_POINT('Ctrl Pts',(-26.7171556987238,22.952879839244,-50.1552101027301));
#17822=CARTESIAN_POINT('Ctrl Pts',(-26.717802349375,22.9563182290865,-50.155426618705));
#17823=CARTESIAN_POINT('Ctrl Pts',(-26.7205499963181,22.971060220494,-50.156353281195));
#17824=CARTESIAN_POINT('Ctrl Pts',(-26.72259612913,22.9823741496658,-50.1570603216025));
#17825=CARTESIAN_POINT('Ctrl Pts',(-26.7566303065972,23.1764896729262,-50.1691240477111));
#17826=CARTESIAN_POINT('Ctrl Pts',(-26.7728355587225,23.3617380754516,-50.1796271695459));
#17827=CARTESIAN_POINT('Ctrl Pts',(-26.7732738217376,23.8527672334791,-50.2071415556081));
#17828=CARTESIAN_POINT('Ctrl Pts',(-26.7301425946833,24.1566006082652,-50.2239916669425));
#17829=CARTESIAN_POINT('Ctrl Pts',(-26.6397864473579,24.4674409269653,-50.2435913330446));
#17830=CARTESIAN_POINT('Ctrl Pts',(-26.6345134267056,24.4850193893926,-50.2447073275911));
#17831=CARTESIAN_POINT('Ctrl Pts',(-26.6273184089501,24.5082812995509,-50.2461945707037));
#17832=CARTESIAN_POINT('Ctrl Pts',(-26.6255301975547,24.5140060323908,-50.2465614209946));
#17833=CARTESIAN_POINT('Ctrl Pts',(-26.6227242115075,24.522901712989,-50.2471327917352));
#17834=CARTESIAN_POINT('Ctrl Pts',(-26.6217174778103,24.5260761519119,-50.2473369484592));
#17835=CARTESIAN_POINT('Ctrl Pts',(-26.6196983835967,24.5324086920071,-50.2477447369298));
#17836=CARTESIAN_POINT('Ctrl Pts',(-26.6186860650631,24.5355668024578,-50.2479483670876));
#17837=CARTESIAN_POINT('Ctrl Pts',(-26.6164026788373,24.5426525921482,-50.2484058376068));
#17838=CARTESIAN_POINT('Ctrl Pts',(-26.6151289371629,24.5465793976186,-50.2486597659605));
#17839=CARTESIAN_POINT('Ctrl Pts',(-26.6113791913829,24.5580642155471,-50.2494036346368));
#17840=CARTESIAN_POINT('Ctrl Pts',(-26.6088827632978,24.5656154822051,-50.249894249397));
#17841=CARTESIAN_POINT('Ctrl Pts',(-26.5903056432636,24.6211178550001,-50.2535116176539));
#17842=CARTESIAN_POINT('Ctrl Pts',(-26.5731268917951,24.6686914415021,-50.2566746412048));
#17843=CARTESIAN_POINT('Ctrl Pts',(-26.5132237490912,24.823106432757,-50.2671553438891));
#17844=CARTESIAN_POINT('Ctrl Pts',(-26.4659009576916,24.9280568257782,-50.2746239359925));
#17845=CARTESIAN_POINT('Ctrl Pts',(-26.2723798936959,25.3023943562076,-50.3025135354043));
#17846=CARTESIAN_POINT('Ctrl Pts',(-26.0936161196279,25.5530659161506,-50.3238439952972));
#17847=CARTESIAN_POINT('Ctrl Pts',(-25.8807558965519,25.7762075686282,-50.3437362181018));
#17848=CARTESIAN_POINT('Ctrl Pts',(-25.8793403175193,25.7776886915042,-50.3438682918727));
#17849=CARTESIAN_POINT('Ctrl Pts',(-25.8501560844299,25.8081659678576,-50.3465867440912));
#17850=CARTESIAN_POINT('Ctrl Pts',(-25.8218477741054,25.8366437630058,-50.3491409006351));
#17851=CARTESIAN_POINT('Ctrl Pts',(-25.7891840009625,25.8682973693923,-50.3519882691086));
#17852=CARTESIAN_POINT('Ctrl Pts',(-25.7853456647844,25.8719985731562,-50.3523213396173));
#17853=CARTESIAN_POINT('Ctrl Pts',(-25.7797287683693,25.8773879565007,-50.3528064986618));
#17854=CARTESIAN_POINT('Ctrl Pts',(-25.7779574648793,25.8790836346399,-50.3529591703685));
#17855=CARTESIAN_POINT('Ctrl Pts',(-25.7748199802351,25.8820803101524,-50.3532290191686));
#17856=CARTESIAN_POINT('Ctrl Pts',(-25.7734545911583,25.8833821304019,-50.3533462608763));
#17857=CARTESIAN_POINT('Ctrl Pts',(-25.7706027724896,25.8860963995772,-50.3535907348077));
#17858=CARTESIAN_POINT('Ctrl Pts',(-25.7691161409313,25.8875086260464,-50.3537179496442));
#17859=CARTESIAN_POINT('Ctrl Pts',(-25.7652336482612,25.8911897593421,-50.3540495943589));
#17860=CARTESIAN_POINT('Ctrl Pts',(-25.7628356407964,25.8934564144334,-50.3542538484359));
#17861=CARTESIAN_POINT('Ctrl Pts',(-25.752432847631,25.9032591801555,-50.3551374144098));
#17862=CARTESIAN_POINT('Ctrl Pts',(-25.7443928857226,25.9107581018392,-50.3558138734789));
#17863=CARTESIAN_POINT('Ctrl Pts',(-25.6860587048758,25.9646111901403,-50.3606771931072));
#17864=CARTESIAN_POINT('Ctrl Pts',(-25.6343342714735,26.0093988512965,-50.3647508343422));
#17865=CARTESIAN_POINT('Ctrl Pts',(-25.5191354080867,26.1029004521583,-50.3734196444774));
#17866=CARTESIAN_POINT('Ctrl Pts',(-25.4551939900038,26.1509660253299,-50.377983831344));
#17867=CARTESIAN_POINT('Ctrl Pts',(-25.1092319277721,26.39141743402,-50.4017789993747));
#17868=CARTESIAN_POINT('Ctrl Pts',(-24.7998031977697,26.5404449754087,-50.4203103113212));
#17869=CARTESIAN_POINT('Ctrl Pts',(-24.4534209982649,26.6439253073304,-50.4421752659924));
#17870=CARTESIAN_POINT('Ctrl Pts',(-24.4340384490717,26.6495180810118,-50.4434011861833));
#17871=CARTESIAN_POINT('Ctrl Pts',(-24.40860558306,26.6565986786266,-50.4450133511992));
#17872=CARTESIAN_POINT('Ctrl Pts',(-24.4026013644391,26.6582515361678,-50.4453942118229));
#17873=CARTESIAN_POINT('Ctrl Pts',(-24.3933343153643,26.660773721166,-50.4459824526326));
#17874=CARTESIAN_POINT('Ctrl Pts',(-24.3900748231625,26.6616553475836,-50.4461894325555));
#17875=CARTESIAN_POINT('Ctrl Pts',(-24.3836499279953,26.6633823196646,-50.4465975746036));
#17876=CARTESIAN_POINT('Ctrl Pts',(-24.3804846090037,26.6642279642547,-50.4467987267362));
#17877=CARTESIAN_POINT('Ctrl Pts',(-24.3734989781126,26.666082832643,-50.4472428227357));
#17878=CARTESIAN_POINT('Ctrl Pts',(-24.3696780929086,26.6670898590595,-50.4474858375984));
#17879=CARTESIAN_POINT('Ctrl Pts',(-24.3617571884742,26.669161908222,-50.4479898535839));
#17880=CARTESIAN_POINT('Ctrl Pts',(-24.3576569040913,26.6702258787162,-50.4482508883521));
#17881=CARTESIAN_POINT('Ctrl Pts',(-24.347158771125,26.6729279269138,-50.4489195626694));
#17882=CARTESIAN_POINT('Ctrl Pts',(-24.3407579863139,26.6745544222816,-50.4493275769424));
#17883=CARTESIAN_POINT('Ctrl Pts',(-24.3222768308405,26.6791902165059,-50.4505065894271));
#17884=CARTESIAN_POINT('Ctrl Pts',(-24.3101840653041,26.682149179274,-50.4512792120296));
#17885=CARTESIAN_POINT('Ctrl Pts',(-24.1917834116107,26.7103943727069,-50.4588557694568));
#17886=CARTESIAN_POINT('Ctrl Pts',(-24.0842831083798,26.7303256531529,-50.4658312976475));
#17887=CARTESIAN_POINT('Ctrl Pts',(-23.6808163275798,26.7840961245158,-50.4923907813779));
#17888=CARTESIAN_POINT('Ctrl Pts',(-23.3816742706496,26.7823308358957,-50.512995451743));
#17889=CARTESIAN_POINT('Ctrl Pts',(-22.9976072689334,26.7265507694895,-50.5386695975442));
#17890=CARTESIAN_POINT('Ctrl Pts',(-22.9087351143983,26.7098009572123,-50.5445389936143));
#17891=CARTESIAN_POINT('Ctrl Pts',(-22.8144232653694,26.6878812639749,-50.5506090339629));
#17892=CARTESIAN_POINT('Ctrl Pts',(-22.8081748452796,26.6864093325922,-50.5510104332862));
#17893=CARTESIAN_POINT('Ctrl Pts',(-22.799519813761,26.6843431642154,-50.5515653426784));
#17894=CARTESIAN_POINT('Ctrl Pts',(-22.7971094811021,26.6837648185823,-50.5517197615124));
#17895=CARTESIAN_POINT('Ctrl Pts',(-22.7929692117749,26.6827663313488,-50.5519848046707));
#17896=CARTESIAN_POINT('Ctrl Pts',(-22.7912389564238,26.6823475373166,-50.5520955070968));
#17897=CARTESIAN_POINT('Ctrl Pts',(-22.7876669963338,26.6814798401352,-50.5523239143032));
#17898=CARTESIAN_POINT('Ctrl Pts',(-22.7858253441804,26.6810307465909,-50.5524416071977));
#17899=CARTESIAN_POINT('Ctrl Pts',(-22.7815048873509,26.6799731480659,-50.5527175471227));
#17900=CARTESIAN_POINT('Ctrl Pts',(-22.7790264008944,26.6793633211207,-50.5528757171403));
#17901=CARTESIAN_POINT('Ctrl Pts',(-22.7709896441648,26.6773757635143,-50.5533881975562));
#17902=CARTESIAN_POINT('Ctrl Pts',(-22.7654342805864,26.675986152589,-50.5537418216334));
#17903=CARTESIAN_POINT('Ctrl Pts',(-22.6155969661923,26.6380814055283,-50.5632634913327));
#17904=CARTESIAN_POINT('Ctrl Pts',(-22.4739902523969,26.5916240966747,-50.5718605016207));
#17905=CARTESIAN_POINT('Ctrl Pts',(-22.2472101780383,26.4993885800572,-50.5857134494194));
#17906=CARTESIAN_POINT('Ctrl Pts',(-22.160112839272,26.4593393289906,-50.5910556896339));
#17907=CARTESIAN_POINT('Ctrl Pts',(-22.0750357068432,26.4155366157209,-50.5964032705493));
#17908=CARTESIAN_POINT('',(-26.7730025135596,23.5499106452406,-50.4388495108445));
#17909=CARTESIAN_POINT('Ctrl Pts',(-22.0750360284016,26.415536781278,-50.8458393738826));
#17910=CARTESIAN_POINT('Ctrl Pts',(-22.0956768960379,26.4261639114079,-50.8444417962392));
#17911=CARTESIAN_POINT('Ctrl Pts',(-22.1164336446989,26.4365685430621,-50.8430364980611));
#17912=CARTESIAN_POINT('Ctrl Pts',(-22.1464834693602,26.4512272514963,-50.8410014702696));
#17913=CARTESIAN_POINT('Ctrl Pts',(-22.1556853635674,26.4556620235051,-50.8403782280499));
#17914=CARTESIAN_POINT('Ctrl Pts',(-22.1687212408711,26.4618683529765,-50.8394951535349));
#17915=CARTESIAN_POINT('Ctrl Pts',(-22.1725379286027,26.4636762685401,-50.839236585064));
#17916=CARTESIAN_POINT('Ctrl Pts',(-22.1791982204146,26.4668151481272,-50.8387853340284));
#17917=CARTESIAN_POINT('Ctrl Pts',(-22.1820402429718,26.4681494717756,-50.8385927682097));
#17918=CARTESIAN_POINT('Ctrl Pts',(-22.1879248129586,26.4709017775051,-50.8381940231165));
#17919=CARTESIAN_POINT('Ctrl Pts',(-22.1909676335063,26.4723191626449,-50.837987823499));
#17920=CARTESIAN_POINT('Ctrl Pts',(-22.1981517685009,26.475651975884,-50.8375009464129));
#17921=CARTESIAN_POINT('Ctrl Pts',(-22.2022949391999,26.4775633642484,-50.8372201297208));
#17922=CARTESIAN_POINT('Ctrl Pts',(-22.2110622710138,26.4815854787121,-50.8366258278653));
#17923=CARTESIAN_POINT('Ctrl Pts',(-22.2156873906137,26.4836940743727,-50.8363122700022));
#17924=CARTESIAN_POINT('Ctrl Pts',(-22.2507945630995,26.4995992479001,-50.8339318657707));
#17925=CARTESIAN_POINT('Ctrl Pts',(-22.2814838740098,26.5129308844117,-50.8318490961091));
#17926=CARTESIAN_POINT('Ctrl Pts',(-22.3702613471033,26.5498640446792,-50.8258162338943));
#17927=CARTESIAN_POINT('Ctrl Pts',(-22.4288353212862,26.5722503786448,-50.8218260035584));
#17928=CARTESIAN_POINT('Ctrl Pts',(-22.5620731542152,26.618765368079,-50.8127237181772));
#17929=CARTESIAN_POINT('Ctrl Pts',(-22.637038721028,26.6419039598359,-50.8075842972956));
#17930=CARTESIAN_POINT('Ctrl Pts',(-22.9971138315956,26.7388042961162,-50.7828496390657));
#17931=CARTESIAN_POINT('Ctrl Pts',(-23.290578276944,26.7759897482668,-50.7623901779033));
#17932=CARTESIAN_POINT('Ctrl Pts',(-23.5882462737214,26.7727802015371,-50.7431377838111));
#17933=CARTESIAN_POINT('Ctrl Pts',(-23.591493324781,26.772740282562,-50.7429279716931));
#17934=CARTESIAN_POINT('Ctrl Pts',(-23.5960766206183,26.7726770073656,-50.7426321020325));
#17935=CARTESIAN_POINT('Ctrl Pts',(-23.5974129088404,26.7726577277195,-50.7425458736657));
#17936=CARTESIAN_POINT('Ctrl Pts',(-23.6013447125728,26.7725985543666,-50.7422922627132));
#17937=CARTESIAN_POINT('Ctrl Pts',(-23.6039401986983,26.7725563558673,-50.7421249777092));
#17938=CARTESIAN_POINT('Ctrl Pts',(-23.6459391657969,26.7718227609664,-50.7394201848066));
#17939=CARTESIAN_POINT('Ctrl Pts',(-23.6853290275148,26.7704117460691,-50.7369138269154));
#17940=CARTESIAN_POINT('Ctrl Pts',(-23.7294541178396,26.7680199507212,-50.7341476208134));
#17941=CARTESIAN_POINT('Ctrl Pts',(-23.7342224425952,26.7677508524412,-50.7338492377378));
#17942=CARTESIAN_POINT('Ctrl Pts',(-23.7413973147941,26.7673299396213,-50.7334010985473));
#17943=CARTESIAN_POINT('Ctrl Pts',(-23.7438042921338,26.7671860238301,-50.7332509015141));
#17944=CARTESIAN_POINT('Ctrl Pts',(-23.7479703925729,26.7669322354467,-50.7329911818766));
#17945=CARTESIAN_POINT('Ctrl Pts',(-23.7497295867082,26.7668236211622,-50.7328815881482));
#17946=CARTESIAN_POINT('Ctrl Pts',(-23.7533924879916,26.7665944537024,-50.7326535584582));
#17947=CARTESIAN_POINT('Ctrl Pts',(-23.7552961751057,26.7664736536673,-50.7325351371265));
#17948=CARTESIAN_POINT('Ctrl Pts',(-23.7598155160419,26.7661828463333,-50.7322542183688));
#17949=CARTESIAN_POINT('Ctrl Pts',(-23.7624310794692,26.7660113374825,-50.732091806101));
#17950=CARTESIAN_POINT('Ctrl Pts',(-23.7711431118365,26.7654293929783,-50.7315513911076));
#17951=CARTESIAN_POINT('Ctrl Pts',(-23.7772386704085,26.7650048070667,-50.7311741834696));
#17952=CARTESIAN_POINT('Ctrl Pts',(-23.9311374103601,26.7538450890673,-50.7216725978437));
#17953=CARTESIAN_POINT('Ctrl Pts',(-24.0780497708452,26.7329434927783,-50.713112765683));
#17954=CARTESIAN_POINT('Ctrl Pts',(-24.2969529822255,26.6862166691887,-50.7004469260784));
#17955=CARTESIAN_POINT('Ctrl Pts',(-24.370308865288,26.6678382513418,-50.6962185083487));
#17956=CARTESIAN_POINT('Ctrl Pts',(-24.5361296049185,26.6200355178534,-50.6865743014601));
#17957=CARTESIAN_POINT('Ctrl Pts',(-24.6280462335212,26.5889827557182,-50.6811649761854));
#17958=CARTESIAN_POINT('Ctrl Pts',(-24.8918154783562,26.4863962337935,-50.6651745219889));
#17959=CARTESIAN_POINT('Ctrl Pts',(-25.0590178775955,26.4040819624656,-50.6544159768157));
#17960=CARTESIAN_POINT('Ctrl Pts',(-25.2280973206403,26.3018137124546,-50.6424003194625));
#17961=CARTESIAN_POINT('Ctrl Pts',(-25.2379883096228,26.2957579506732,-50.6416931616399));
#17962=CARTESIAN_POINT('Ctrl Pts',(-25.2516369872835,26.2872999160644,-50.6407113615871));
#17963=CARTESIAN_POINT('Ctrl Pts',(-25.2554227838812,26.2849429823193,-50.6404383938511));
#17964=CARTESIAN_POINT('Ctrl Pts',(-25.2619174534283,26.2808808483826,-50.6399689997531));
#17965=CARTESIAN_POINT('Ctrl Pts',(-25.2646287079938,26.2791794516062,-50.6397727144357));
#17966=CARTESIAN_POINT('Ctrl Pts',(-25.2701458810268,26.2757057863946,-50.6393726098349));
#17967=CARTESIAN_POINT('Ctrl Pts',(-25.2729516046243,26.2739332179408,-50.6391687795936));
#17968=CARTESIAN_POINT('Ctrl Pts',(-25.2794166703331,26.2698348055958,-50.6386982726403));
#17969=CARTESIAN_POINT('Ctrl Pts',(-25.2830740604103,26.2675059082123,-50.638431482486));
#17970=CARTESIAN_POINT('Ctrl Pts',(-25.2907438706796,26.2626002602529,-50.637870702135));
#17971=CARTESIAN_POINT('Ctrl Pts',(-25.2947552910684,26.2600219727802,-50.6375766549293));
#17972=CARTESIAN_POINT('Ctrl Pts',(-25.3053742358064,26.2531634340918,-50.6367962574583));
#17973=CARTESIAN_POINT('Ctrl Pts',(-25.3119717930802,26.2488678775412,-50.636309334412));
#17974=CARTESIAN_POINT('Ctrl Pts',(-25.4471803020444,26.1601287914516,-50.6262877503444));
#17975=CARTESIAN_POINT('Ctrl Pts',(-25.5695766385052,26.0666202562459,-50.616404789033));
#17976=CARTESIAN_POINT('Ctrl Pts',(-25.9416694005638,25.7376667219318,-50.5836004305717));
#17977=CARTESIAN_POINT('Ctrl Pts',(-26.1606189150832,25.4710904597472,-50.5595541428315));
#17978=CARTESIAN_POINT('Ctrl Pts',(-26.3345797123176,25.1731033444322,-50.537745502929));
#17979=CARTESIAN_POINT('Ctrl Pts',(-26.335710276104,25.1711620798558,-50.5376036350083));
#17980=CARTESIAN_POINT('Ctrl Pts',(-26.3432850657636,25.158124257781,-50.5366522222086));
#17981=CARTESIAN_POINT('Ctrl Pts',(-26.3496651229148,25.1469902625698,-50.535846506356));
#17982=CARTESIAN_POINT('Ctrl Pts',(-26.3577749224714,25.1326396265604,-50.5348169772922));
#17983=CARTESIAN_POINT('Ctrl Pts',(-26.3595658191417,25.1294579477183,-50.5345892832113));
#17984=CARTESIAN_POINT('Ctrl Pts',(-26.3622885884199,25.1246014293397,-50.5342425962013));
#17985=CARTESIAN_POINT('Ctrl Pts',(-26.3632243725285,25.1229288043453,-50.5341233505836));
#17986=CARTESIAN_POINT('Ctrl Pts',(-26.3649761414641,25.1197911184493,-50.5338999513798));
#17987=CARTESIAN_POINT('Ctrl Pts',(-26.3657924719637,25.1183262606664,-50.5337957756199));
#17988=CARTESIAN_POINT('Ctrl Pts',(-26.3676634252024,25.1149627721575,-50.5335568513913));
#17989=CARTESIAN_POINT('Ctrl Pts',(-26.3687172703442,25.1130637155943,-50.5334221537534));
#17990=CARTESIAN_POINT('Ctrl Pts',(-26.3716307350508,25.1078010439874,-50.5330494320366));
#17991=CARTESIAN_POINT('Ctrl Pts',(-26.3734862661872,25.1044351513719,-50.5328116718754));
#17992=CARTESIAN_POINT('Ctrl Pts',(-26.3835712364906,25.0860635788879,-50.5315172979406));
#17993=CARTESIAN_POINT('Ctrl Pts',(-26.3916872706754,25.0709954784822,-50.5304678709575));
#17994=CARTESIAN_POINT('Ctrl Pts',(-26.4833367007158,24.8975451180664,-50.5185187838262));
#17995=CARTESIAN_POINT('Ctrl Pts',(-26.5536634684481,24.7325054650257,-50.5083857883047));
#17996=CARTESIAN_POINT('Ctrl Pts',(-26.6733032548985,24.3708607447798,-50.4870404757371));
#17997=CARTESIAN_POINT('Ctrl Pts',(-26.7185475392238,24.1737473751388,-50.4758838170986));
#17998=CARTESIAN_POINT('Ctrl Pts',(-26.7593915971981,23.8655895963788,-50.4579020537943));
#17999=CARTESIAN_POINT('Ctrl Pts',(-26.768222768076,23.7568309416626,-50.4514617962942));
#18000=CARTESIAN_POINT('Ctrl Pts',(-26.771950602867,23.6337809247315,-50.4439882212096));
#18001=CARTESIAN_POINT('Ctrl Pts',(-26.7722845086353,23.6197175156082,-50.4431313724413));
#18002=CARTESIAN_POINT('Ctrl Pts',(-26.7726187430012,23.6002771832538,-50.4419430587074));
#18003=CARTESIAN_POINT('Ctrl Pts',(-26.7726977094018,23.5949016263272,-50.4416140633374));
#18004=CARTESIAN_POINT('Ctrl Pts',(-26.7728023016572,23.5863194883079,-50.4410881588143));
#18005=CARTESIAN_POINT('Ctrl Pts',(-26.77283659333,23.5831130067104,-50.4408915219491));
#18006=CARTESIAN_POINT('Ctrl Pts',(-26.7728958080148,23.5766779111493,-50.4404965938168));
#18007=CARTESIAN_POINT('Ctrl Pts',(-26.7729206649192,23.5734493002506,-50.4402983006936));
#18008=CARTESIAN_POINT('Ctrl Pts',(-26.7729609906621,23.5669410663189,-50.439898276714));
#18009=CARTESIAN_POINT('Ctrl Pts',(-26.7729763050827,23.5636614466582,-50.4396965412549));
#18010=CARTESIAN_POINT('Ctrl Pts',(-26.772997583751,23.5568914254722,-50.4392797806001));
#18011=CARTESIAN_POINT('Ctrl Pts',(-26.7730028838382,23.5534010296548,-50.4390647349235));
#18012=CARTESIAN_POINT('Ctrl Pts',(-26.7730025135596,23.5499106452406,-50.4388495108445));
#18013=CARTESIAN_POINT('Ctrl Pts',(-26.7730025136018,23.5499110428036,-50.4388495353591));
#18014=CARTESIAN_POINT('Ctrl Pts',(-26.7730020002086,23.5450659720061,-50.438550778629));
#18015=CARTESIAN_POINT('Ctrl Pts',(-26.7729905607256,23.540220929427,-50.4382516785179));
#18016=CARTESIAN_POINT('Ctrl Pts',(-26.7728798798832,23.5162441225703,-50.4367697892271));
#18017=CARTESIAN_POINT('Ctrl Pts',(-26.7726212019504,23.4971138010535,-50.4355820031528));
#18018=CARTESIAN_POINT('Ctrl Pts',(-26.7679256386955,23.2877626462575,-50.422522228925));
#18019=CARTESIAN_POINT('Ctrl Pts',(-26.7468224487095,23.0983244634533,-50.4101158335791));
#18020=CARTESIAN_POINT('Ctrl Pts',(-26.650632902803,22.6223437056152,-50.3775986227797));
#18021=CARTESIAN_POINT('Ctrl Pts',(-26.5525937045061,22.3422243301948,-50.3570929796435));
#18022=CARTESIAN_POINT('Ctrl Pts',(-26.4120233109153,22.068178321527,-50.3376681968354));
#18023=CARTESIAN_POINT('Ctrl Pts',(-26.4062135782473,22.0570136123423,-50.3368782619577));
#18024=CARTESIAN_POINT('Ctrl Pts',(-26.398720963306,22.0428185650594,-50.3358760358632));
#18025=CARTESIAN_POINT('Ctrl Pts',(-26.3970984993017,22.0397567168573,-50.3356599833889));
#18026=CARTESIAN_POINT('Ctrl Pts',(-26.3944906508888,22.0348544183463,-50.3353142731019));
#18027=CARTESIAN_POINT('Ctrl Pts',(-26.3935084167594,22.0330123092114,-50.3351844149724));
#18028=CARTESIAN_POINT('Ctrl Pts',(-26.3916398712976,22.0295161738203,-50.3349380495827));
#18029=CARTESIAN_POINT('Ctrl Pts',(-26.3907539118305,22.0278619795431,-50.3348215214092));
#18030=CARTESIAN_POINT('Ctrl Pts',(-26.3887220668953,22.0240762257711,-50.3345549265203));
#18031=CARTESIAN_POINT('Ctrl Pts',(-26.3875752265068,22.0219451854384,-50.334404921986));
#18032=CARTESIAN_POINT('Ctrl Pts',(-26.3840379300535,22.0153899429654,-50.3339436890125));
#18033=CARTESIAN_POINT('Ctrl Pts',(-26.3816395038037,22.0109700153203,-50.333632968857));
#18034=CARTESIAN_POINT('Ctrl Pts',(-26.3635086965006,21.9777435055112,-50.3312990484874));
#18035=CARTESIAN_POINT('Ctrl Pts',(-26.3473466800712,21.9491718295774,-50.3293028488182));
#18036=CARTESIAN_POINT('Ctrl Pts',(-26.3264923106088,21.9135848269859,-50.3268237435692));
#18037=CARTESIAN_POINT('Ctrl Pts',(-26.3222058991371,21.9063355576893,-50.3263191182778));
#18038=CARTESIAN_POINT('Ctrl Pts',(-26.1901947753866,21.6850599623424,-50.3109251116409));
#18039=CARTESIAN_POINT('Ctrl Pts',(-26.0380820088197,21.486523530566,-50.2973245438593));
#18040=CARTESIAN_POINT('Ctrl Pts',(-25.7133344992387,21.1514133043372,-50.2711313247174));
#18041=CARTESIAN_POINT('Ctrl Pts',(-25.5467122623584,21.0110636318964,-50.2586960517792));
#18042=CARTESIAN_POINT('Ctrl Pts',(-25.3569658949198,20.8815338321716,-50.2447317633018));
#18043=CARTESIAN_POINT('Ctrl Pts',(-25.3466392148444,20.8745717675132,-50.2439725241306));
#18044=CARTESIAN_POINT('Ctrl Pts',(-25.3331143765499,20.8655671497709,-50.2429790297503));
#18045=CARTESIAN_POINT('Ctrl Pts',(-25.3299525016519,20.8634700740895,-50.2427468302474));
#18046=CARTESIAN_POINT('Ctrl Pts',(-25.3237524759972,20.859373727748,-50.2422916357075));
#18047=CARTESIAN_POINT('Ctrl Pts',(-25.3207146287371,20.8573740062624,-50.2420686580513));
#18048=CARTESIAN_POINT('Ctrl Pts',(-25.3176684801766,20.8553762028834,-50.2418451250709));
#18049=CARTESIAN_POINT('Ctrl Pts',(-25.3176635475717,20.8553729678751,-50.2418447631059));
#18050=CARTESIAN_POINT('Ctrl Pts',(-25.3176536763093,20.8553664939278,-50.2418440387318));
#18051=CARTESIAN_POINT('Ctrl Pts',(-25.317648736119,20.8553632539835,-50.2418436762104));
#18052=CARTESIAN_POINT('Ctrl Pts',(-25.3176388439939,20.8553567664315,-50.2418429503059));
#18053=CARTESIAN_POINT('Ctrl Pts',(-25.3176338935312,20.8553535197893,-50.241842587031));
#18054=CARTESIAN_POINT('Ctrl Pts',(-25.3176239887374,20.8553470240067,-50.2418418601974));
#18055=CARTESIAN_POINT('Ctrl Pts',(-25.3176190310386,20.8553437726579,-50.2418414963918));
#18056=CARTESIAN_POINT('Ctrl Pts',(-25.3176091048279,20.8553372629081,-50.2418407679872));
#18057=CARTESIAN_POINT('Ctrl Pts',(-25.317604137428,20.8553340052364,-50.2418404034699));
#18058=CARTESIAN_POINT('Ctrl Pts',(-25.3175941967233,20.8553274860598,-50.2418396740023));
#18059=CARTESIAN_POINT('Ctrl Pts',(-25.3175892218346,20.8553242235162,-50.2418393089358));
#18060=CARTESIAN_POINT('Ctrl Pts',(-25.3175792602737,20.8553176907409,-50.2418385779383));
#18061=CARTESIAN_POINT('Ctrl Pts',(-25.3175742761751,20.855314422197,-50.2418382121963));
#18062=CARTESIAN_POINT('Ctrl Pts',(-25.3175642957918,20.8553078771571,-50.2418374798182));
#18063=CARTESIAN_POINT('Ctrl Pts',(-25.3175593012948,20.8553046018337,-50.2418371133133));
#18064=CARTESIAN_POINT('Ctrl Pts',(-25.3175493070174,20.8552980477617,-50.2418363799162));
#18065=CARTESIAN_POINT('Ctrl Pts',(-25.3175443048984,20.8552947674796,-50.2418360128523));
#18066=CARTESIAN_POINT('Ctrl Pts',(-25.3175342884258,20.8552881989321,-50.2418352778271));
#18067=CARTESIAN_POINT('Ctrl Pts',(-25.3175292761578,20.8552849120346,-50.2418349100187));
#18068=CARTESIAN_POINT('Ctrl Pts',(-25.3175192435097,20.8552783329597,-50.2418341738071));
#18069=CARTESIAN_POINT('Ctrl Pts',(-25.3175142222856,20.855275040229,-50.2418338053418));
#18070=CARTESIAN_POINT('Ctrl Pts',(-25.3175041704501,20.855268448652,-50.2418330677228));
#18071=CARTESIAN_POINT('Ctrl Pts',(-25.317499139872,20.8552651498276,-50.2418326985714));
#18072=CARTESIAN_POINT('Ctrl Pts',(-25.3174890689219,20.8552585457967,-50.2418319595503));
#18073=CARTESIAN_POINT('Ctrl Pts',(-25.3174840284966,20.8552552405553,-50.2418315896766));
#18074=CARTESIAN_POINT('Ctrl Pts',(-25.3174739400269,20.8552486251169,-50.2418308493705));
#18075=CARTESIAN_POINT('Ctrl Pts',(-25.3174688905957,20.8552453140105,-50.2418304788362));
#18076=CARTESIAN_POINT('Ctrl Pts',(-25.3174587822177,20.8552386855986,-50.2418297370698));
#18077=CARTESIAN_POINT('Ctrl Pts',(-25.3174537233094,20.8552353683184,-50.2418293658404));
#18078=CARTESIAN_POINT('Ctrl Pts',(-25.3174435949174,20.8552287268641,-50.2418286226059));
#18079=CARTESIAN_POINT('Ctrl Pts',(-25.3174385257194,20.8552254028775,-50.2418282506217));
#18080=CARTESIAN_POINT('Ctrl Pts',(-25.3174283800736,20.8552187501914,-50.2418275061217));
#18081=CARTESIAN_POINT('Ctrl Pts',(-25.3174233019599,20.8552154203995,-50.2418271334836));
#18082=CARTESIAN_POINT('Ctrl Pts',(-25.3174131352233,20.855208753966,-50.2418263874365));
#18083=CARTESIAN_POINT('Ctrl Pts',(-25.3174080473457,20.855205417813,-50.2418260140822));
#18084=CARTESIAN_POINT('Ctrl Pts',(-25.317397859896,20.8551987378801,-50.2418252665157));
#18085=CARTESIAN_POINT('Ctrl Pts',(-25.3173927611784,20.8551953946606,-50.2418248923663));
#18086=CARTESIAN_POINT('Ctrl Pts',(-25.3173825573834,20.8551887040929,-50.241824143601));
#18087=CARTESIAN_POINT('Ctrl Pts',(-25.3173774502884,20.8551853554218,-50.2418237688371));
#18088=CARTESIAN_POINT('Ctrl Pts',(-25.3173672216869,20.8551786486718,-50.2418230182522));
#18089=CARTESIAN_POINT('Ctrl Pts',(-25.3173621029243,20.8551752923921,-50.2418226426324));
#18090=CARTESIAN_POINT('Ctrl Pts',(-25.317351858965,20.8551685756556,-50.241821890921));
#18091=CARTESIAN_POINT('Ctrl Pts',(-25.317346731654,20.8551652138127,-50.2418215146743));
#18092=CARTESIAN_POINT('Ctrl Pts',(-25.3173364624011,20.8551584805755,-50.2418207611075));
#18093=CARTESIAN_POINT('Ctrl Pts',(-25.3173313230958,20.8551551109102,-50.2418203839809));
#18094=CARTESIAN_POINT('Ctrl Pts',(-25.3173210376342,20.8551483671297,-50.2418196292253));
#18095=CARTESIAN_POINT('Ctrl Pts',(-25.3173158887848,20.8551449912488,-50.2418192513987));
#18096=CARTESIAN_POINT('Ctrl Pts',(-25.3173055818222,20.8551382334554,-50.2418184950659));
#18097=CARTESIAN_POINT('Ctrl Pts',(-25.3173004232899,20.8551348512681,-50.2418181165291));
#18098=CARTESIAN_POINT('Ctrl Pts',(-25.3172900935528,20.8551280786274,-50.2418173585257));
#18099=CARTESIAN_POINT('Ctrl Pts',(-25.3172849240483,20.8551246892886,-50.241816979184));
#18100=CARTESIAN_POINT('Ctrl Pts',(-25.3172745746714,20.8551179038563,-50.2418162197401));
#18101=CARTESIAN_POINT('Ctrl Pts',(-25.3172693950126,20.8551145079027,-50.2418158396536));
#18102=CARTESIAN_POINT('Ctrl Pts',(-25.3172590230613,20.8551077077552,-50.2418150785538));
#18103=CARTESIAN_POINT('Ctrl Pts',(-25.3172538322125,20.855104304508,-50.2418146976465));
#18104=CARTESIAN_POINT('Ctrl Pts',(-25.3172434404056,20.8550974914284,-50.2418139350903));
#18105=CARTESIAN_POINT('Ctrl Pts',(-25.3172382392833,20.8550940814886,-50.2418135534294));
#18106=CARTESIAN_POINT('Ctrl Pts',(-25.3172278240575,20.8550872531414,-50.2418127891554));
#18107=CARTESIAN_POINT('Ctrl Pts',(-25.317222611199,20.8550838355504,-50.2418124066336));
#18108=CARTESIAN_POINT('Ctrl Pts',(-25.3172121760735,20.8550769942432,-50.2418116408999));
#18109=CARTESIAN_POINT('Ctrl Pts',(-25.3172069523462,20.8550735695699,-50.2418112575809));
#18110=CARTESIAN_POINT('Ctrl Pts',(-25.3171964960468,20.855066714468,-50.2418104902941));
#18111=CARTESIAN_POINT('Ctrl Pts',(-25.3171912621843,20.8550632831936,-50.2418101062317));
#18112=CARTESIAN_POINT('Ctrl Pts',(-25.3171807803602,20.8550564114452,-50.2418093370725));
#18113=CARTESIAN_POINT('Ctrl Pts',(-25.317175533757,20.8550529718618,-50.2418089520755));
#18114=CARTESIAN_POINT('Ctrl Pts',(-25.3171650344398,20.8550460887328,-50.2418081816333));
#18115=CARTESIAN_POINT('Ctrl Pts',(-25.3171597781994,20.8550426428753,-50.2418077959294));
#18116=CARTESIAN_POINT('Ctrl Pts',(-25.3171492537723,20.8550357433728,-50.2418070236453));
#18117=CARTESIAN_POINT('Ctrl Pts',(-25.3171439867632,20.8550322904998,-50.2418066371516));
#18118=CARTESIAN_POINT('Ctrl Pts',(-25.3171334365432,20.8550253741767,-50.2418058629754));
#18119=CARTESIAN_POINT('Ctrl Pts',(-25.3171281561072,20.8550219125458,-50.2418054754967));
#18120=CARTESIAN_POINT('Ctrl Pts',(-25.3171175889064,20.8550149851795,-50.2418047000752));
#18121=CARTESIAN_POINT('Ctrl Pts',(-25.3171122988296,20.855011517273,-50.2418043118893));
#18122=CARTESIAN_POINT('Ctrl Pts',(-25.317101704821,20.8550045724219,-50.2418035345013));
#18123=CARTESIAN_POINT('Ctrl Pts',(-25.317096403136,20.8550010969503,-50.241803145464));
#18124=CARTESIAN_POINT('Ctrl Pts',(-25.3170857835668,20.8549941354328,-50.241802366201));
#18125=CARTESIAN_POINT('Ctrl Pts',(-25.3170804678823,20.8549906508289,-50.2418019761367));
#18126=CARTESIAN_POINT('Ctrl Pts',(-25.3170673903863,20.8549820781606,-50.241801016512));
#18127=CARTESIAN_POINT('Ctrl Pts',(-25.3170596238428,20.8549769870198,-50.2418004466046));
#18128=CARTESIAN_POINT('Ctrl Pts',(-25.3170440162035,20.854966755964,-50.2417993013198));
#18129=CARTESIAN_POINT('Ctrl Pts',(-25.3170361764729,20.8549616169449,-50.2417987260427));
#18130=CARTESIAN_POINT('Ctrl Pts',(-25.3170204225301,20.8549512901813,-50.2417975700236));
#18131=CARTESIAN_POINT('Ctrl Pts',(-25.3170125083478,20.8549461024575,-50.2417969892839));
#18132=CARTESIAN_POINT('Ctrl Pts',(-25.3169966059355,20.854935678572,-50.2417958223717));
#18133=CARTESIAN_POINT('Ctrl Pts',(-25.3169886165374,20.8549304416456,-50.2417952361134));
#18134=CARTESIAN_POINT('Ctrl Pts',(-25.3169725626485,20.8549199186726,-50.2417940580874));
#18135=CARTESIAN_POINT('Ctrl Pts',(-25.3169644975312,20.8549146322164,-50.2417934662736));
#18136=CARTESIAN_POINT('Ctrl Pts',(-25.3169482859129,20.8549040060633,-50.241792276675));
#18137=CARTESIAN_POINT('Ctrl Pts',(-25.316940141956,20.8548986680351,-50.2417916790769));
#18138=CARTESIAN_POINT('Ctrl Pts',(-25.3169237726923,20.8548879387631,-50.2417904779119));
#18139=CARTESIAN_POINT('Ctrl Pts',(-25.3169155479906,20.854882547917,-50.2417898743894));
#18140=CARTESIAN_POINT('Ctrl Pts',(-25.3168990215729,20.8548717158543,-50.2417886616942));
#18141=CARTESIAN_POINT('Ctrl Pts',(-25.316890717171,20.8548662728782,-50.2417880523242));
#18142=CARTESIAN_POINT('Ctrl Pts',(-25.3168740235799,20.8548553314641,-50.2417868273635));
#18143=CARTESIAN_POINT('Ctrl Pts',(-25.3168656360262,20.8548498340991,-50.2417862118928));
#18144=CARTESIAN_POINT('Ctrl Pts',(-25.3168487761526,20.8548387839241,-50.2417849747321));
#18145=CARTESIAN_POINT('Ctrl Pts',(-25.3168403040439,20.8548332312537,-50.2417843530576));
#18146=CARTESIAN_POINT('Ctrl Pts',(-25.3168232747434,20.8548220702637,-50.2417831034662));
#18147=CARTESIAN_POINT('Ctrl Pts',(-25.316814716858,20.8548164614907,-50.2417824754983));
#18148=CARTESIAN_POINT('Ctrl Pts',(-25.3167975138016,20.8548051868555,-50.2417812131586));
#18149=CARTESIAN_POINT('Ctrl Pts',(-25.3167888682306,20.8547995207323,-50.2417805787573));
#18150=CARTESIAN_POINT('Ctrl Pts',(-25.3167714892016,20.8547881310063,-50.2417793035067));
#18151=CARTESIAN_POINT('Ctrl Pts',(-25.3167627549109,20.8547824068589,-50.2417786625962));
#18152=CARTESIAN_POINT('Ctrl Pts',(-25.3167451948876,20.8547708987582,-50.2417773740662));
#18153=CARTESIAN_POINT('Ctrl Pts',(-25.3167363699281,20.8547651153129,-50.2417767265034));
#18154=CARTESIAN_POINT('Ctrl Pts',(-25.3167186243574,20.8547534858615,-50.2417754243601));
#18155=CARTESIAN_POINT('Ctrl Pts',(-25.3167097055671,20.85474764105,-50.241774769913));
#18156=CARTESIAN_POINT('Ctrl Pts',(-25.3166917750511,20.8547358906503,-50.2417734542005));
#18157=CARTESIAN_POINT('Ctrl Pts',(-25.3166827621516,20.8547299842941,-50.2417727928488));
#18158=CARTESIAN_POINT('Ctrl Pts',(-25.3166646385515,20.8547181076204,-50.24177146297));
#18159=CARTESIAN_POINT('Ctrl Pts',(-25.3166555284443,20.8547121376933,-50.2417707944863));
#18160=CARTESIAN_POINT('Ctrl Pts',(-25.3166372117029,20.8547001347166,-50.241769450437));
#18161=CARTESIAN_POINT('Ctrl Pts',(-25.3166280039023,20.8546941009042,-50.2417687747858));
#18162=CARTESIAN_POINT('Ctrl Pts',(-25.3166094849838,20.8546819657121,-50.2417674159031));
#18163=CARTESIAN_POINT('Ctrl Pts',(-25.3166001754163,20.8546758653497,-50.2417667327854));
#18164=CARTESIAN_POINT('Ctrl Pts',(-25.3165814563936,20.8546635993091,-50.2417653592214));
#18165=CARTESIAN_POINT('Ctrl Pts',(-25.3165720451032,20.85465743243,-50.2417646686406));
#18166=CARTESIAN_POINT('Ctrl Pts',(-25.3165531156774,20.8546450288018,-50.2417632796397));
#18167=CARTESIAN_POINT('Ctrl Pts',(-25.3165435987515,20.8546387928468,-50.2417625813085));
#18168=CARTESIAN_POINT('Ctrl Pts',(-25.3165244594839,20.8546262520081,-50.2417611769121));
#18169=CARTESIAN_POINT('Ctrl Pts',(-25.3165148361539,20.8546199464784,-50.2417604707743));
#18170=CARTESIAN_POINT('Ctrl Pts',(-25.3164954783713,20.854607262756,-50.2417590503458));
#18171=CARTESIAN_POINT('Ctrl Pts',(-25.3164857451203,20.8546008853522,-50.2417583361434));
#18172=CARTESIAN_POINT('Ctrl Pts',(-25.3164661668358,20.8545880574544,-50.2417568995372));
#18173=CARTESIAN_POINT('Ctrl Pts',(-25.3164563215481,20.8545816067955,-50.2417561771149));
#18174=CARTESIAN_POINT('Ctrl Pts',(-25.3164365182896,20.8545686318024,-50.241754724003));
#18175=CARTESIAN_POINT('Ctrl Pts',(-25.3164265593842,20.8545621068577,-50.2417539932448));
#18176=CARTESIAN_POINT('Ctrl Pts',(-25.3164065228835,20.854548979363,-50.2417525230205));
#18177=CARTESIAN_POINT('Ctrl Pts',(-25.3163964462786,20.8545423774637,-50.241751783627));
#18178=CARTESIAN_POINT('Ctrl Pts',(-25.3163761763708,20.8545290973704,-50.2417502962783));
#18179=CARTESIAN_POINT('Ctrl Pts',(-25.3163659813274,20.8545224180379,-50.2417495481953));
#18180=CARTESIAN_POINT('Ctrl Pts',(-25.3163454674766,20.8545089784548,-50.2417480429491));
#18181=CARTESIAN_POINT('Ctrl Pts',(-25.316335149813,20.8545022189555,-50.2417472858699));
#18182=CARTESIAN_POINT('Ctrl Pts',(-25.3163143900167,20.8544886185827,-50.2417457625794));
#18183=CARTESIAN_POINT('Ctrl Pts',(-25.3163039474617,20.8544817774346,-50.2417449963373));
#18184=CARTESIAN_POINT('Ctrl Pts',(-25.3162829355784,20.8544680122609,-50.241743454552));
#18185=CARTESIAN_POINT('Ctrl Pts',(-25.3162723658106,20.8544610879495,-50.2417426789766));
#18186=CARTESIAN_POINT('Ctrl Pts',(-25.3162510940008,20.854447152852,-50.2417411181214));
#18187=CARTESIAN_POINT('Ctrl Pts',(-25.3162403931832,20.8544401428702,-50.2417403329313));
#18188=CARTESIAN_POINT('Ctrl Pts',(-25.3162130384493,20.8544222233332,-50.2417383257346));
#18189=CARTESIAN_POINT('Ctrl Pts',(-25.3161963847925,20.8544113140776,-50.2417371037478));
#18190=CARTESIAN_POINT('Ctrl Pts',(-25.3161621888355,20.8543889138985,-50.2417345945721));
#18191=CARTESIAN_POINT('Ctrl Pts',(-25.3161446457126,20.8543774224602,-50.2417333073229));
#18192=CARTESIAN_POINT('Ctrl Pts',(-25.3161086033742,20.8543538138081,-50.2417306626737));
#18193=CARTESIAN_POINT('Ctrl Pts',(-25.3160901048937,20.8543416971031,-50.2417293053278));
#18194=CARTESIAN_POINT('Ctrl Pts',(-25.3160520663688,20.8543167820168,-50.2417265142142));
#18195=CARTESIAN_POINT('Ctrl Pts',(-25.3160325260867,20.8543039835123,-50.2417250804291));
#18196=CARTESIAN_POINT('Ctrl Pts',(-25.3132022331559,20.8524502404983,-50.241517405584));
#18197=CARTESIAN_POINT('Ctrl Pts',(-25.3103885668257,20.8506136688153,-50.2413109964285));
#18198=CARTESIAN_POINT('Ctrl Pts',(-25.3037494041122,20.8462948624852,-50.2408240555912));
#18199=CARTESIAN_POINT('Ctrl Pts',(-25.2999215087333,20.8438163456926,-50.240543385359));
#18200=CARTESIAN_POINT('Ctrl Pts',(-25.2876680888495,20.8359192627766,-50.2396451881001));
#18201=CARTESIAN_POINT('Ctrl Pts',(-25.2792226172716,20.830531893,-50.2390265000034));
#18202=CARTESIAN_POINT('Ctrl Pts',(-25.1923656756222,20.7756938795585,-50.232667237762));
#18203=CARTESIAN_POINT('Ctrl Pts',(-25.1118876241331,20.7296135494006,-50.2268030202967));
#18204=CARTESIAN_POINT('Ctrl Pts',(-24.7705435170173,20.5532550727604,-50.2020061750991));
#18205=CARTESIAN_POINT('Ctrl Pts',(-24.4946061995773,20.4552166954043,-50.1819770665401));
#18206=CARTESIAN_POINT('Ctrl Pts',(-24.1619521466171,20.3857171687362,-50.159233896628));
#18207=CARTESIAN_POINT('Ctrl Pts',(-24.1143525715086,20.3768864974977,-50.1560163074523));
#18208=CARTESIAN_POINT('Ctrl Pts',(-23.9972707340411,20.3578833096796,-50.1482174639488));
#18209=CARTESIAN_POINT('Ctrl Pts',(-23.9276156883753,20.348901988529,-50.1436764124958));
#18210=CARTESIAN_POINT('Ctrl Pts',(-23.8465975529191,20.3411370817139,-50.1385500225014));
#18211=CARTESIAN_POINT('Ctrl Pts',(-23.8354723295114,20.3401291666838,-50.1378494680136));
#18212=CARTESIAN_POINT('Ctrl Pts',(-23.8210347256364,20.3388968081694,-50.1369449250092));
#18213=CARTESIAN_POINT('Ctrl Pts',(-23.8177271022499,20.3386196239797,-50.1367380085852));
#18214=CARTESIAN_POINT('Ctrl Pts',(-23.8123710462274,20.3381791095128,-50.1364034597079));
#18215=CARTESIAN_POINT('Ctrl Pts',(-23.8103228861163,20.3380126284564,-50.1362756491896));
#18216=CARTESIAN_POINT('Ctrl Pts',(-23.8063953621675,20.3376971676469,-50.1360307957626));
#18217=CARTESIAN_POINT('Ctrl Pts',(-23.8045160325539,20.3375478784749,-50.135913735879));
#18218=CARTESIAN_POINT('Ctrl Pts',(-23.8002009847008,20.3372089120075,-50.1356451946692));
#18219=CARTESIAN_POINT('Ctrl Pts',(-23.7977651753108,20.3370203548177,-50.1354937770644));
#18220=CARTESIAN_POINT('Ctrl Pts',(-23.7900605607506,20.3364327497014,-50.1350153703267));
#18221=CARTESIAN_POINT('Ctrl Pts',(-23.7847909527081,20.3360438869517,-50.1346889550394));
#18222=CARTESIAN_POINT('Ctrl Pts',(-23.7407378759118,20.3329019712742,-50.1319666276001));
#18223=CARTESIAN_POINT('Ctrl Pts',(-23.701906368189,20.3308378736766,-50.1296087597192));
#18224=CARTESIAN_POINT('Ctrl Pts',(-23.6545350688029,20.3291789185289,-50.1267729262057));
#18225=CARTESIAN_POINT('Ctrl Pts',(-23.646023975837,20.3289146260291,-50.1262650135649));
#18226=CARTESIAN_POINT('Ctrl Pts',(-23.6307030236759,20.328499643136,-50.1253534237588));
#18227=CARTESIAN_POINT('Ctrl Pts',(-23.6238935784234,20.3283368043207,-50.1249492286689));
#18228=CARTESIAN_POINT('Ctrl Pts',(-23.2898947997024,20.321409086965,-50.1051687871448));
#18229=CARTESIAN_POINT('Ctrl Pts',(-22.9635481752055,20.3644945939467,-50.0877812691631));
#18230=CARTESIAN_POINT('Ctrl Pts',(-22.5240788380082,20.4924621811883,-50.0614472605143));
#18231=CARTESIAN_POINT('Ctrl Pts',(-22.4012478275343,20.5364682089086,-50.053769557474));
#18232=CARTESIAN_POINT('Ctrl Pts',(-22.2726711430846,20.5915375871081,-50.0452505704415));
#18233=CARTESIAN_POINT('Ctrl Pts',(-22.263930260567,20.5953272636757,-50.0446690122715));
#18234=CARTESIAN_POINT('Ctrl Pts',(-22.2511889896193,20.6009185859215,-50.043817707755));
#18235=CARTESIAN_POINT('Ctrl Pts',(-22.2471752156891,20.6026897557305,-50.0435490065917));
#18236=CARTESIAN_POINT('Ctrl Pts',(-22.2401247505953,20.6058181508242,-50.0430760914124));
#18237=CARTESIAN_POINT('Ctrl Pts',(-22.2370865140661,20.6071718946628,-50.042871997264));
#18238=CARTESIAN_POINT('Ctrl Pts',(-22.2311430464702,20.6098311548748,-50.0424721493944));
#18239=CARTESIAN_POINT('Ctrl Pts',(-22.2282376433837,20.6111362797852,-50.0422764093245));
#18240=CARTESIAN_POINT('Ctrl Pts',(-22.2207061464996,20.6145329014726,-50.0417682788296));
#18241=CARTESIAN_POINT('Ctrl Pts',(-22.2160830648774,20.6166310204909,-50.0414556603345));
#18242=CARTESIAN_POINT('Ctrl Pts',(-22.1997527663674,20.6240888772935,-50.0403488540552));
#18243=CARTESIAN_POINT('Ctrl Pts',(-22.1880728508341,20.6295077880025,-50.039552623334));
#18244=CARTESIAN_POINT('Ctrl Pts',(-21.9873743675207,20.7240877924514,-50.0257901834959));
#18245=CARTESIAN_POINT('Ctrl Pts',(-21.8074753929521,20.831338691536,-50.012167152358));
#18246=CARTESIAN_POINT('Ctrl Pts',(-21.4117530127917,21.122752107863,-49.9792070801838));
#18247=CARTESIAN_POINT('Ctrl Pts',(-21.2072704939656,21.3194710233723,-49.9596439535045));
#18248=CARTESIAN_POINT('Ctrl Pts',(-21.0201796111594,21.5539678151568,-49.9406445867811));
#18249=CARTESIAN_POINT('Ctrl Pts',(-21.009414551862,21.567687514963,-49.9395472483268));
#18250=CARTESIAN_POINT('Ctrl Pts',(-20.9963991267586,21.5845553785613,-49.9382161227806));
#18251=CARTESIAN_POINT('Ctrl Pts',(-20.9940426477454,21.5876207421544,-49.9379749401167));
#18252=CARTESIAN_POINT('Ctrl Pts',(-20.9903680187879,21.5924186311604,-49.9375985764283));
#18253=CARTESIAN_POINT('Ctrl Pts',(-20.9890461080359,21.5941482509935,-49.9374631284888));
#18254=CARTESIAN_POINT('Ctrl Pts',(-20.9867089210746,21.5972127134853,-49.9372235562282));
#18255=CARTESIAN_POINT('Ctrl Pts',(-20.9856929398078,21.598547001972,-49.9371193817052));
#18256=CARTESIAN_POINT('Ctrl Pts',(-20.9835204976667,21.6014046961486,-49.9368965599921));
#18257=CARTESIAN_POINT('Ctrl Pts',(-20.9823643545868,21.6029283341004,-49.9367779355847));
#18258=CARTESIAN_POINT('Ctrl Pts',(-20.9790171240451,21.6073476892115,-49.9364343734598));
#18259=CARTESIAN_POINT('Ctrl Pts',(-20.9768295644485,21.6102460934441,-49.9362096860037));
#18260=CARTESIAN_POINT('Ctrl Pts',(-20.9670424276813,21.623259230776,-49.9352037082689));
#18261=CARTESIAN_POINT('Ctrl Pts',(-20.9594974165506,21.6334151444595,-49.934426217781));
#18262=CARTESIAN_POINT('Ctrl Pts',(-20.9505359937039,21.6456271850315,-49.9335000420566));
#18263=CARTESIAN_POINT('Ctrl Pts',(-20.949062057381,21.6476406675715,-49.9333476193017));
#18264=CARTESIAN_POINT('Ctrl Pts',(-20.7458123518565,21.9259692109315,-49.9123164835966));
#18265=CARTESIAN_POINT('Ctrl Pts',(-20.5892825295412,22.2327034267842,-49.8942103961434));
#18266=CARTESIAN_POINT('Ctrl Pts',(-20.4499226741283,22.6635252302605,-49.8683969487487));
#18267=CARTESIAN_POINT('Ctrl Pts',(-20.4213438088466,22.770344059194,-49.8619885794897));
#18268=CARTESIAN_POINT('Ctrl Pts',(-20.388010474822,22.9267277684508,-49.852462266578));
#18269=CARTESIAN_POINT('Ctrl Pts',(-20.3788248170785,22.9752709685916,-49.8494860659408));
#18270=CARTESIAN_POINT('Ctrl Pts',(-20.3694678225881,23.0318041701198,-49.8459917853832));
#18271=CARTESIAN_POINT('Ctrl Pts',(-20.3682055342755,23.0396088459752,-49.845508766755));
#18272=CARTESIAN_POINT('Ctrl Pts',(-20.366338220827,23.0514301959241,-49.8447762037539));
#18273=CARTESIAN_POINT('Ctrl Pts',(-20.3657120433869,23.0554435385461,-49.8445273318617));
#18274=CARTESIAN_POINT('Ctrl Pts',(-20.3645935109586,23.0627025925342,-49.8440768836937));
#18275=CARTESIAN_POINT('Ctrl Pts',(-20.3640985239652,23.0659478977344,-49.8438753913066));
#18276=CARTESIAN_POINT('Ctrl Pts',(-20.3630417931978,23.0729479282544,-49.8434405372689));
#18277=CARTESIAN_POINT('Ctrl Pts',(-20.3624817243261,23.076702898027,-49.843207122772));
#18278=CARTESIAN_POINT('Ctrl Pts',(-20.3610302424024,23.0865535942789,-49.8425943931043));
#18279=CARTESIAN_POINT('Ctrl Pts',(-20.36014967387,23.0926508809827,-49.8422147344845));
#18280=CARTESIAN_POINT('Ctrl Pts',(-20.3563922652732,23.1192061680272,-49.840559463026));
#18281=CARTESIAN_POINT('Ctrl Pts',(-20.3536947489173,23.1396886774523,-49.8392781814762));
#18282=CARTESIAN_POINT('Ctrl Pts',(-20.3095087415122,23.5020806693544,-49.8165247135761));
#18283=CARTESIAN_POINT('Ctrl Pts',(-20.3229102067689,23.8483743413689,-49.7930996990299));
#18284=CARTESIAN_POINT('Ctrl Pts',(-20.4182598044101,24.3223432656205,-49.7605507383427));
#18285=CARTESIAN_POINT('Ctrl Pts',(-20.4545391319408,24.4569336796419,-49.7513007592741));
#18286=CARTESIAN_POINT('Ctrl Pts',(-20.5044837763894,24.6036553632162,-49.7414987900895));
#18287=CARTESIAN_POINT('Ctrl Pts',(-20.5096600760049,24.6185045519117,-49.740510132091));
#18288=CARTESIAN_POINT('Ctrl Pts',(-20.5162016786626,24.6368375338564,-49.7392942222472));
#18289=CARTESIAN_POINT('Ctrl Pts',(-20.5174645119276,24.6403572850109,-49.739060994819));
#18290=CARTESIAN_POINT('Ctrl Pts',(-20.5194626737804,24.6458961859858,-49.7386943216765));
#18291=CARTESIAN_POINT('Ctrl Pts',(-20.5201938954758,24.6479167978367,-49.7385606309943));
#18292=CARTESIAN_POINT('Ctrl Pts',(-20.5215641657706,24.651691513139,-49.738311021361));
#18293=CARTESIAN_POINT('Ctrl Pts',(-20.5222027132966,24.6534457808833,-49.7381950735894));
#18294=CARTESIAN_POINT('Ctrl Pts',(-20.5236393598822,24.6573820040369,-49.737935035595));
#18295=CARTESIAN_POINT('Ctrl Pts',(-20.5244382925804,24.6595636471099,-49.7377909964453));
#18296=CARTESIAN_POINT('Ctrl Pts',(-20.5264742844153,24.6651047595953,-49.7374253691098));
#18297=CARTESIAN_POINT('Ctrl Pts',(-20.5277145870833,24.6684630451683,-49.737203975308));
#18298=CARTESIAN_POINT('Ctrl Pts',(-20.5345743312589,24.686941919117,-49.7359868322829));
#18299=CARTESIAN_POINT('Ctrl Pts',(-20.5403017725884,24.7020225718351,-49.7349974680043));
#18300=CARTESIAN_POINT('Ctrl Pts',(-20.6622212337014,25.0159214111125,-49.7144742219785));
#18301=CARTESIAN_POINT('Ctrl Pts',(-20.8222680473139,25.2958447536944,-49.6973660628039));
#18302=CARTESIAN_POINT('Ctrl Pts',(-21.0991314900078,25.6464388991739,-49.6720461834813));
#18303=CARTESIAN_POINT('Ctrl Pts',(-21.1829393425262,25.7406440667304,-49.664783428253));
#18304=CARTESIAN_POINT('Ctrl Pts',(-21.3098639827515,25.8675001418701,-49.6541133903177));
#18305=CARTESIAN_POINT('Ctrl Pts',(-21.3486212761428,25.9043546183876,-49.6508952996255));
#18306=CARTESIAN_POINT('Ctrl Pts',(-21.3942567741854,25.9456366135999,-49.6471432601842));
#18307=CARTESIAN_POINT('Ctrl Pts',(-21.4002579565977,25.9510244765975,-49.6466505802782));
#18308=CARTESIAN_POINT('Ctrl Pts',(-21.4093366251953,25.9591139666523,-49.6459063058606));
#18309=CARTESIAN_POINT('Ctrl Pts',(-21.4123991715399,25.9618323752324,-49.645655416949));
#18310=CARTESIAN_POINT('Ctrl Pts',(-21.4179289871208,25.9667219946389,-49.6452027257308));
#18311=CARTESIAN_POINT('Ctrl Pts',(-21.4203944162299,25.9688952857916,-49.6450010108997));
#18312=CARTESIAN_POINT('Ctrl Pts',(-21.4253391362841,25.9732406640172,-49.6445966735427));
#18313=CARTESIAN_POINT('Ctrl Pts',(-21.4278184437906,25.9754127263514,-49.6443940503254));
#18314=CARTESIAN_POINT('Ctrl Pts',(-21.434521208968,25.9812667082719,-49.6438465651668));
#18315=CARTESIAN_POINT('Ctrl Pts',(-21.4387509292319,25.9849414109663,-49.6435014036081));
#18316=CARTESIAN_POINT('Ctrl Pts',(-21.4553368811333,25.9992752497532,-49.6421491704837));
#18317=CARTESIAN_POINT('Ctrl Pts',(-21.4677642507908,26.0098513609089,-49.6411386727369));
#18318=CARTESIAN_POINT('Ctrl Pts',(-21.6633696427828,26.1737729801621,-49.6252736036894));
#18319=CARTESIAN_POINT('Ctrl Pts',(-21.8628644390159,26.3062983933942,-49.6095527808294));
#18320=CARTESIAN_POINT('Ctrl Pts',(-22.0750360207194,26.4155367773228,-49.5934531403533));
#18321=CARTESIAN_POINT('Origin',(-23.5502525316942,23.5502525316942,-77.3107734492734));
#18322=CARTESIAN_POINT('',(-22.0750360039475,26.4155367686876,-48.0944001480293));
#18323=CARTESIAN_POINT('',(-22.0750360153631,26.415536774565,-48.3398410585546));
#18324=CARTESIAN_POINT('',(-22.0750360153461,26.4155367745563,-77.3107734492734));
#18325=CARTESIAN_POINT('',(-26.7730021298787,23.5518618488042,-48.9415966136197));
#18326=CARTESIAN_POINT('Ctrl Pts',(-22.0750360039475,26.4155367686876,-48.0944001480293));
#18327=CARTESIAN_POINT('Ctrl Pts',(-22.0625887732288,26.4091282036162,-48.09532660084));
#18328=CARTESIAN_POINT('Ctrl Pts',(-22.0501825072825,26.4026381203314,-48.0962551212754));
#18329=CARTESIAN_POINT('Ctrl Pts',(-21.7725163997001,26.2550698835405,-48.1171500683835));
#18330=CARTESIAN_POINT('Ctrl Pts',(-21.5282523406975,26.0776798282403,-48.1380504180745));
#18331=CARTESIAN_POINT('Ctrl Pts',(-21.2870403498004,25.8448550398867,-48.1595706989458));
#18332=CARTESIAN_POINT('Ctrl Pts',(-21.262378884575,25.8202667324444,-48.1617807350983));
#18333=CARTESIAN_POINT('Ctrl Pts',(-21.2349097336589,25.7919765382236,-48.1642485383034));
#18334=CARTESIAN_POINT('Ctrl Pts',(-21.2317069554985,25.7886638445665,-48.1645363694615));
#18335=CARTESIAN_POINT('Ctrl Pts',(-21.22686887767,25.783638205244,-48.164971293972));
#18336=CARTESIAN_POINT('Ctrl Pts',(-21.2252283603404,25.7819303250401,-48.1651187929188));
#18337=CARTESIAN_POINT('Ctrl Pts',(-21.2223778179862,25.7789561789583,-48.165375122372));
#18338=CARTESIAN_POINT('Ctrl Pts',(-21.2211669428764,25.777690735112,-48.1654840196397));
#18339=CARTESIAN_POINT('Ctrl Pts',(-21.2187446984804,25.7751551962392,-48.1657018808578));
#18340=CARTESIAN_POINT('Ctrl Pts',(-21.2175333362632,25.7738850998876,-48.1658108441033));
#18341=CARTESIAN_POINT('Ctrl Pts',(-21.2145903253526,25.7707943425504,-48.1660755995659));
#18342=CARTESIAN_POINT('Ctrl Pts',(-21.2128597630664,25.7689726404851,-48.1662313064656));
#18343=CARTESIAN_POINT('Ctrl Pts',(-21.2092051600506,25.7651165471217,-48.1665601845476));
#18344=CARTESIAN_POINT('Ctrl Pts',(-21.2072816344027,25.7630816660154,-48.1667333158049));
#18345=CARTESIAN_POINT('Ctrl Pts',(-21.2021069081029,25.7575930562424,-48.1671991762352));
#18346=CARTESIAN_POINT('Ctrl Pts',(-21.1988606605349,25.7541346360319,-48.1674915272791));
#18347=CARTESIAN_POINT('Ctrl Pts',(-21.1161145471454,25.6655893439804,-48.1749465463505));
#18348=CARTESIAN_POINT('Ctrl Pts',(-21.0412662040387,25.5762515719009,-48.1817631982991));
#18349=CARTESIAN_POINT('Ctrl Pts',(-20.8000529502861,25.2544113876788,-48.2047711065651));
#18350=CARTESIAN_POINT('Ctrl Pts',(-20.6598605958874,25.0040072646886,-48.220201212852));
#18351=CARTESIAN_POINT('Ctrl Pts',(-20.5156234243607,24.6403312462466,-48.2429112139811));
#18352=CARTESIAN_POINT('Ctrl Pts',(-20.4815743555706,24.540432334521,-48.2491621203294));
#18353=CARTESIAN_POINT('Ctrl Pts',(-20.4496334201428,24.4291073033612,-48.256210759028));
#18354=CARTESIAN_POINT('Ctrl Pts',(-20.446828266588,24.4191497703988,-48.256841913022));
#18355=CARTESIAN_POINT('Ctrl Pts',(-20.4429394427688,24.4050864102072,-48.2577343328712));
#18356=CARTESIAN_POINT('Ctrl Pts',(-20.4418158484235,24.4009916093653,-48.2579942986));
#18357=CARTESIAN_POINT('Ctrl Pts',(-20.4398740573298,24.3938597872687,-48.258447291053));
#18358=CARTESIAN_POINT('Ctrl Pts',(-20.4390522059858,24.3908237592847,-48.2586401987118));
#18359=CARTESIAN_POINT('Ctrl Pts',(-20.4373456507233,24.3844827269534,-48.2590432487689));
#18360=CARTESIAN_POINT('Ctrl Pts',(-20.4364617631893,24.3811775091202,-48.2592534173823));
#18361=CARTESIAN_POINT('Ctrl Pts',(-20.4343826351071,24.3733528923157,-48.2597511567321));
#18362=CARTESIAN_POINT('Ctrl Pts',(-20.4331919638677,24.3688322970479,-48.2600388753806));
#18363=CARTESIAN_POINT('Ctrl Pts',(-20.4292874430094,24.3538760417347,-48.2609913051552));
#18364=CARTESIAN_POINT('Ctrl Pts',(-20.4266161535181,24.343429436979,-48.2616573941101));
#18365=CARTESIAN_POINT('Ctrl Pts',(-20.384303960178,24.1744300662099,-48.2724470963648));
#18366=CARTESIAN_POINT('Ctrl Pts',(-20.3567341204745,24.0131272109517,-48.2829643848882));
#18367=CARTESIAN_POINT('Ctrl Pts',(-20.3104686642528,23.5186082854301,-48.3158572334247));
#18368=CARTESIAN_POINT('Ctrl Pts',(-20.3310855188014,23.1839900232791,-48.3391900229575));
#18369=CARTESIAN_POINT('Ctrl Pts',(-20.4059707817135,22.8432494438367,-48.3612573309848));
#18370=CARTESIAN_POINT('Ctrl Pts',(-20.409431204229,22.8280319961916,-48.3622386839533));
#18371=CARTESIAN_POINT('Ctrl Pts',(-20.4138114167834,22.8093968067229,-48.3634348108927));
#18372=CARTESIAN_POINT('Ctrl Pts',(-20.4146263957595,22.8059550048508,-48.363655491745));
#18373=CARTESIAN_POINT('Ctrl Pts',(-20.415982969897,22.8002677239412,-48.3640197491373));
#18374=CARTESIAN_POINT('Ctrl Pts',(-20.4165213130549,22.7980214852302,-48.3641635127119));
#18375=CARTESIAN_POINT('Ctrl Pts',(-20.4174723178158,22.7940721532068,-48.3644160941215));
#18376=CARTESIAN_POINT('Ctrl Pts',(-20.4178839526641,22.7923688213315,-48.3645249713726));
#18377=CARTESIAN_POINT('Ctrl Pts',(-20.4187860226274,22.7886493736889,-48.3647625872896));
#18378=CARTESIAN_POINT('Ctrl Pts',(-20.4192770144226,22.7866334001925,-48.3648912928893));
#18379=CARTESIAN_POINT('Ctrl Pts',(-20.4205950058017,22.7812444733419,-48.3652351155361));
#18380=CARTESIAN_POINT('Ctrl Pts',(-20.4214255140287,22.7778723681848,-48.3654500288049));
#18381=CARTESIAN_POINT('Ctrl Pts',(-20.423267937923,22.7704433272696,-48.365923001553));
#18382=CARTESIAN_POINT('Ctrl Pts',(-20.4242823032629,22.7663869970449,-48.3661809204885));
#18383=CARTESIAN_POINT('Ctrl Pts',(-20.4273336801604,22.7542850131336,-48.3669494659465));
#18384=CARTESIAN_POINT('Ctrl Pts',(-20.4293938990702,22.7462451669669,-48.3674587867714));
#18385=CARTESIAN_POINT('Ctrl Pts',(-20.4367885328502,22.7178448870333,-48.3692537795239));
#18386=CARTESIAN_POINT('Ctrl Pts',(-20.4422914520189,22.6975283449827,-48.3705302927805));
#18387=CARTESIAN_POINT('Ctrl Pts',(-20.4735865563069,22.5863174720065,-48.3774835663004));
#18388=CARTESIAN_POINT('Ctrl Pts',(-20.5031695499096,22.4965291778998,-48.3829719226044));
#18389=CARTESIAN_POINT('Ctrl Pts',(-20.6436884877099,22.1257463939698,-48.4055988094271));
#18390=CARTESIAN_POINT('Ctrl Pts',(-20.7898794208234,21.8597838920622,-48.4218895392893));
#18391=CARTESIAN_POINT('Ctrl Pts',(-20.9831712292851,21.6017593739134,-48.4407770982359));
#18392=CARTESIAN_POINT('Ctrl Pts',(-20.9955306148411,21.5855826099918,-48.4419748928928));
#18393=CARTESIAN_POINT('Ctrl Pts',(-21.0108214617046,21.5659572282934,-48.4434454501685));
#18394=CARTESIAN_POINT('Ctrl Pts',(-21.0136081694865,21.5623960505268,-48.4437130021893));
#18395=CARTESIAN_POINT('Ctrl Pts',(-21.0188889274124,21.5556768728978,-48.4442191654296));
#18396=CARTESIAN_POINT('Ctrl Pts',(-21.0213814172274,21.5525176539001,-48.4444577196151));
#18397=CARTESIAN_POINT('Ctrl Pts',(-21.0265627685202,21.545975550922,-48.4449529013298));
#18398=CARTESIAN_POINT('Ctrl Pts',(-21.0292525288564,21.5425933918409,-48.4452095616096));
#18399=CARTESIAN_POINT('Ctrl Pts',(-21.0648210393213,21.4980530112639,-48.4485983461633));
#18400=CARTESIAN_POINT('Ctrl Pts',(-21.0986957539248,21.4577035008415,-48.4517674378346));
#18401=CARTESIAN_POINT('Ctrl Pts',(-21.1393109565201,21.4116655430357,-48.4555088065573));
#18402=CARTESIAN_POINT('Ctrl Pts',(-21.1451057131952,21.4051505839833,-48.4560412666273));
#18403=CARTESIAN_POINT('Ctrl Pts',(-21.1537878382799,21.395468806964,-48.4568370851176));
#18404=CARTESIAN_POINT('Ctrl Pts',(-21.1566552339007,21.39228406509,-48.457099600796));
#18405=CARTESIAN_POINT('Ctrl Pts',(-21.1617836452282,21.3866108687821,-48.4575685611331));
#18406=CARTESIAN_POINT('Ctrl Pts',(-21.1640422232325,21.384120210999,-48.4577749023314));
#18407=CARTESIAN_POINT('Ctrl Pts',(-21.1688150903041,21.3788734323361,-48.458210545946));
#18408=CARTESIAN_POINT('Ctrl Pts',(-21.1713302741994,21.376118135436,-48.4584398862504));
#18409=CARTESIAN_POINT('Ctrl Pts',(-21.1779930961137,21.3688446491991,-48.4590468066445));
#18410=CARTESIAN_POINT('Ctrl Pts',(-21.1821488428739,21.3643339381333,-48.4594247325239));
#18411=CARTESIAN_POINT('Ctrl Pts',(-21.2010751421603,21.3439083591188,-48.4611431088836));
#18412=CARTESIAN_POINT('Ctrl Pts',(-21.2159931471152,21.3281314495534,-48.4624898828902));
#18413=CARTESIAN_POINT('Ctrl Pts',(-21.3269650247111,21.2131210039306,-48.4724542191031));
#18414=CARTESIAN_POINT('Ctrl Pts',(-21.4291368776997,21.1200158376521,-48.4813439936919));
#18415=CARTESIAN_POINT('Ctrl Pts',(-21.6481939454459,20.9447610228789,-48.4998574208491));
#18416=CARTESIAN_POINT('Ctrl Pts',(-21.7652069971699,20.8632430439146,-48.5094755387822));
#18417=CARTESIAN_POINT('Ctrl Pts',(-22.0563389884322,20.6878546586753,-48.5324827293605));
#18418=CARTESIAN_POINT('Ctrl Pts',(-22.2344827127081,20.6017162144219,-48.5458572541248));
#18419=CARTESIAN_POINT('Ctrl Pts',(-22.4249222868872,20.5303545062692,-48.5587596223211));
#18420=CARTESIAN_POINT('Ctrl Pts',(-22.4304426190029,20.5283031600954,-48.5591324440799));
#18421=CARTESIAN_POINT('Ctrl Pts',(-22.449146118309,20.521411259232,-48.5603915302762));
#18422=CARTESIAN_POINT('Ctrl Pts',(-22.4623555328882,20.5166416593952,-48.5612739246607));
#18423=CARTESIAN_POINT('Ctrl Pts',(-22.479115737028,20.5107135093853,-48.562384493903));
#18424=CARTESIAN_POINT('Ctrl Pts',(-22.4826376673603,20.5094746702226,-48.562617362655));
#18425=CARTESIAN_POINT('Ctrl Pts',(-22.4882096922287,20.5075255842298,-48.5629849800685));
#18426=CARTESIAN_POINT('Ctrl Pts',(-22.4902583509053,20.5068112875683,-48.563119970085));
#18427=CARTESIAN_POINT('Ctrl Pts',(-22.4938945406286,20.5055475904437,-48.563359259596));
#18428=CARTESIAN_POINT('Ctrl Pts',(-22.4954817712766,20.5049973654464,-48.5634636081955));
#18429=CARTESIAN_POINT('Ctrl Pts',(-22.4991197230587,20.5037394285934,-48.5637025396719));
#18430=CARTESIAN_POINT('Ctrl Pts',(-22.5011707251942,20.5030325474968,-48.5638370722662));
#18431=CARTESIAN_POINT('Ctrl Pts',(-22.5069079002291,20.5010617000299,-48.5642129173741));
#18432=CARTESIAN_POINT('Ctrl Pts',(-22.5105956699819,20.4998023422652,-48.5644539549664));
#18433=CARTESIAN_POINT('Ctrl Pts',(-22.5188404542173,20.4970034712504,-48.5649916360898));
#18434=CARTESIAN_POINT('Ctrl Pts',(-22.5233986607553,20.4954674611691,-48.5652880742313));
#18435=CARTESIAN_POINT('Ctrl Pts',(-22.5374883148152,20.49075467372,-48.5662018864853));
#18436=CARTESIAN_POINT('Ctrl Pts',(-22.5470313014161,20.4876122212475,-48.5668172963515));
#18437=CARTESIAN_POINT('Ctrl Pts',(-22.5825547126252,20.4760984135653,-48.5690956188059));
#18438=CARTESIAN_POINT('Ctrl Pts',(-22.6086272902514,20.4680123356921,-48.5707429860009));
#18439=CARTESIAN_POINT('Ctrl Pts',(-22.7018437899409,20.4403957016421,-48.5765551328132));
#18440=CARTESIAN_POINT('Ctrl Pts',(-22.7695206058325,20.4227190136458,-48.5806325251765));
#18441=CARTESIAN_POINT('Ctrl Pts',(-23.2166397810928,20.3213553717628,-48.6069611290282));
#18442=CARTESIAN_POINT('Ctrl Pts',(-23.6079464127548,20.3046736333209,-48.6276040647128));
#18443=CARTESIAN_POINT('Ctrl Pts',(-24.0121987978122,20.360721994616,-48.6522972937338));
#18444=CARTESIAN_POINT('Ctrl Pts',(-24.031529155098,20.3635815123814,-48.6534850407414));
#18445=CARTESIAN_POINT('Ctrl Pts',(-24.0569071133381,20.3675718193061,-48.6550539394472));
#18446=CARTESIAN_POINT('Ctrl Pts',(-24.062979459188,20.3685444245444,-48.6554300607141));
#18447=CARTESIAN_POINT('Ctrl Pts',(-24.0723660559536,20.3700754413111,-48.6560125943732));
#18448=CARTESIAN_POINT('Ctrl Pts',(-24.0756823025816,20.3706216703927,-48.6562186190283));
#18449=CARTESIAN_POINT('Ctrl Pts',(-24.0822969828859,20.3717218253803,-48.6566299989592));
#18450=CARTESIAN_POINT('Ctrl Pts',(-24.0855954209009,20.3722757004591,-48.6568353523844));
#18451=CARTESIAN_POINT('Ctrl Pts',(-24.0929235467024,20.3735179749072,-48.6572920704274));
#18452=CARTESIAN_POINT('Ctrl Pts',(-24.0969527938465,20.374208908264,-48.6575435154686));
#18453=CARTESIAN_POINT('Ctrl Pts',(-24.108629193469,20.3762340495094,-48.6582731329766));
#18454=CARTESIAN_POINT('Ctrl Pts',(-24.1162728141645,20.3775882160427,-48.6587519409795));
#18455=CARTESIAN_POINT('Ctrl Pts',(-24.1692344630231,20.387168541915,-48.6620778511232));
#18456=CARTESIAN_POINT('Ctrl Pts',(-24.2143745220704,20.3963374116326,-48.664954927293));
#18457=CARTESIAN_POINT('Ctrl Pts',(-24.3503745488949,20.4270108386525,-48.6737576984558));
#18458=CARTESIAN_POINT('Ctrl Pts',(-24.4405045843798,20.4514975542336,-48.679776584192));
#18459=CARTESIAN_POINT('Ctrl Pts',(-24.6692783356723,20.5244562754472,-48.6955300152039));
#18460=CARTESIAN_POINT('Ctrl Pts',(-24.8058973144251,20.5785507954279,-48.705408106444));
#18461=CARTESIAN_POINT('Ctrl Pts',(-25.0003587387974,20.6713583912824,-48.7199892998986));
#18462=CARTESIAN_POINT('Ctrl Pts',(-25.0614122450346,20.7029316945391,-48.7246454100565));
#18463=CARTESIAN_POINT('Ctrl Pts',(-25.2065567813154,20.7839763093766,-48.7358506145005));
#18464=CARTESIAN_POINT('Ctrl Pts',(-25.289507715626,20.8353635974676,-48.7423704001027));
#18465=CARTESIAN_POINT('Ctrl Pts',(-25.3734414090793,20.8927880985035,-48.7490032681743));
#18466=CARTESIAN_POINT('Ctrl Pts',(-25.3768730131422,20.8951456575032,-48.7492745127282));
#18467=CARTESIAN_POINT('Ctrl Pts',(-25.3888199373307,20.9033874818409,-48.7502190243816));
#18468=CARTESIAN_POINT('Ctrl Pts',(-25.3973115601326,20.9093061770784,-48.7508907008086));
#18469=CARTESIAN_POINT('Ctrl Pts',(-25.4118141828719,20.9195187280865,-48.7520382250619));
#18470=CARTESIAN_POINT('Ctrl Pts',(-25.4178391578042,20.9237924953388,-48.7525150678665));
#18471=CARTESIAN_POINT('Ctrl Pts',(-25.4561739757982,20.951183594443,-48.7555495205143));
#18472=CARTESIAN_POINT('Ctrl Pts',(-25.4880705438722,20.9748772962822,-48.7580764957407));
#18473=CARTESIAN_POINT('Ctrl Pts',(-25.5237307965886,21.0024045452112,-48.7608965171035));
#18474=CARTESIAN_POINT('Ctrl Pts',(-25.5279310202789,21.0056634448298,-48.7612285892539));
#18475=CARTESIAN_POINT('Ctrl Pts',(-25.5340544512918,21.0104388565594,-48.7617125664865));
#18476=CARTESIAN_POINT('Ctrl Pts',(-25.5359839964076,21.0119471696969,-48.7618650507402));
#18477=CARTESIAN_POINT('Ctrl Pts',(-25.5393964527488,21.0146209375752,-48.7621346833478));
#18478=CARTESIAN_POINT('Ctrl Pts',(-25.5408800611607,21.0157854952609,-48.7622518959708));
#18479=CARTESIAN_POINT('Ctrl Pts',(-25.5437358951059,21.0180312352415,-48.7624774943016));
#18480=CARTESIAN_POINT('Ctrl Pts',(-25.5451082591138,21.0191122271626,-48.762585893148));
#18481=CARTESIAN_POINT('Ctrl Pts',(-25.5488029996504,21.0220273939485,-48.7628776994782));
#18482=CARTESIAN_POINT('Ctrl Pts',(-25.5511237370934,21.0238636582883,-48.7630609567088));
#18483=CARTESIAN_POINT('Ctrl Pts',(-25.5599125367578,21.0308374297148,-48.7637548580096));
#18484=CARTESIAN_POINT('Ctrl Pts',(-25.566363441161,21.0359966584179,-48.7642639555229));
#18485=CARTESIAN_POINT('Ctrl Pts',(-25.5823665541918,21.0488966350769,-48.7655265542763));
#18486=CARTESIAN_POINT('Ctrl Pts',(-25.5918945289732,21.0566674242728,-48.7662779733475));
#18487=CARTESIAN_POINT('Ctrl Pts',(-25.6291144126728,21.0873794219178,-48.7692131290252));
#18488=CARTESIAN_POINT('Ctrl Pts',(-25.6564671443365,21.110729848832,-48.7713697897656));
#18489=CARTESIAN_POINT('Ctrl Pts',(-25.7326571568299,21.178008556507,-48.7773948749799));
#18490=CARTESIAN_POINT('Ctrl Pts',(-25.780552275895,21.2229804138201,-48.781203831528));
#18491=CARTESIAN_POINT('Ctrl Pts',(-26.0239842128392,21.4659773572458,-48.8008858703337));
#18492=CARTESIAN_POINT('Ctrl Pts',(-26.1946361767158,21.6872443632114,-48.8159300031509));
#18493=CARTESIAN_POINT('Ctrl Pts',(-26.3553867082756,21.9631103889067,-48.8344043131287));
#18494=CARTESIAN_POINT('Ctrl Pts',(-26.3753468596096,21.998917694892,-48.8367947850814));
#18495=CARTESIAN_POINT('Ctrl Pts',(-26.3978515975773,22.0411652491172,-48.8396118650846));
#18496=CARTESIAN_POINT('Ctrl Pts',(-26.4010656923614,22.0472458156652,-48.8400172375522));
#18497=CARTESIAN_POINT('Ctrl Pts',(-26.4101184150067,22.0645056630013,-48.84116772132));
#18498=CARTESIAN_POINT('Ctrl Pts',(-26.4159108747056,22.0757089130765,-48.8419142837949));
#18499=CARTESIAN_POINT('Ctrl Pts',(-26.4231847823085,22.0899821936172,-48.8428653050112));
#18500=CARTESIAN_POINT('Ctrl Pts',(-26.42472737604,22.0930210655285,-48.8430677764194));
#18501=CARTESIAN_POINT('Ctrl Pts',(-26.4294217000084,22.1023052260808,-48.8436863386655));
#18502=CARTESIAN_POINT('Ctrl Pts',(-26.4325579044372,22.1085583072656,-48.8441029329401));
#18503=CARTESIAN_POINT('Ctrl Pts',(-26.4364017761514,22.1162850379191,-48.844617701473));
#18504=CARTESIAN_POINT('Ctrl Pts',(-26.4371287308447,22.1177491127632,-48.844715240581));
#18505=CARTESIAN_POINT('Ctrl Pts',(-26.4431758367006,22.1299511825295,-48.8455281633168));
#18506=CARTESIAN_POINT('Ctrl Pts',(-26.4484371175296,22.1407181150175,-48.8462454784779));
#18507=CARTESIAN_POINT('Ctrl Pts',(-26.4588291086963,22.1622889504617,-48.8476827455507));
#18508=CARTESIAN_POINT('Ctrl Pts',(-26.4639599695666,22.1730925672083,-48.8484026780558));
#18509=CARTESIAN_POINT('Ctrl Pts',(-26.4789994741936,22.2052202630491,-48.8505440886882));
#18510=CARTESIAN_POINT('Ctrl Pts',(-26.4887348483143,22.2266241524303,-48.8519713567779));
#18511=CARTESIAN_POINT('Ctrl Pts',(-26.5008732996909,22.2541054388927,-48.8538053349721));
#18512=CARTESIAN_POINT('Ctrl Pts',(-26.5034934843897,22.2600866210292,-48.8542045790501));
#18513=CARTESIAN_POINT('Ctrl Pts',(-26.5076325470082,22.269613672577,-48.8548406629974));
#18514=CARTESIAN_POINT('Ctrl Pts',(-26.5091632775615,22.2731543991117,-48.8550770969578));
#18515=CARTESIAN_POINT('Ctrl Pts',(-26.5118772925569,22.2794632489935,-48.8554984368283));
#18516=CARTESIAN_POINT('Ctrl Pts',(-26.5130630643143,22.2822303028363,-48.8556832574976));
#18517=CARTESIAN_POINT('Ctrl Pts',(-26.5157954745657,22.2886312676377,-48.8561108507973));
#18518=CARTESIAN_POINT('Ctrl Pts',(-26.517339311495,22.2922663629126,-48.8563537186633));
#18519=CARTESIAN_POINT('Ctrl Pts',(-26.5216470289197,22.3024612931751,-48.8570349750167));
#18520=CARTESIAN_POINT('Ctrl Pts',(-26.5243958505806,22.3090274310425,-48.8574738753375));
#18521=CARTESIAN_POINT('Ctrl Pts',(-26.5401471669495,22.3470055045489,-48.8600132587494));
#18522=CARTESIAN_POINT('Ctrl Pts',(-26.5526733159221,22.3786115329793,-48.8621298278362));
#18523=CARTESIAN_POINT('Ctrl Pts',(-26.5873490281897,22.4703153366671,-48.868282806512));
#18524=CARTESIAN_POINT('Ctrl Pts',(-26.6082090823643,22.5308800413996,-48.872361260698));
#18525=CARTESIAN_POINT('Ctrl Pts',(-26.7240475078328,22.9028518982277,-48.8975094081118));
#18526=CARTESIAN_POINT('Ctrl Pts',(-26.7731646259633,23.226454141433,-48.9200696560392));
#18527=CARTESIAN_POINT('Ctrl Pts',(-26.7730021298787,23.5518618488042,-48.9415966136197));
#18528=CARTESIAN_POINT('Ctrl Pts',(-26.7730021275415,23.5518665225018,-48.9415969228025));
#18529=CARTESIAN_POINT('Ctrl Pts',(-26.7729567465358,23.6424814237964,-48.9475914394289));
#18530=CARTESIAN_POINT('Ctrl Pts',(-26.7690895901357,23.7330660802197,-48.9534754575283));
#18531=CARTESIAN_POINT('Ctrl Pts',(-26.7610384286827,23.82772417437,-48.9594298922931));
#18532=CARTESIAN_POINT('Ctrl Pts',(-26.7606599341482,23.8320696702523,-48.9597028119813));
#18533=CARTESIAN_POINT('Ctrl Pts',(-26.7600379551602,23.8390467177372,-48.9601402979653));
#18534=CARTESIAN_POINT('Ctrl Pts',(-26.75980005591,23.8416787427777,-48.9603051733615));
#18535=CARTESIAN_POINT('Ctrl Pts',(-26.7593827892507,23.84623273136,-48.9605901605202));
#18536=CARTESIAN_POINT('Ctrl Pts',(-26.759204932593,23.8481548267028,-48.9607103570862));
#18537=CARTESIAN_POINT('Ctrl Pts',(-26.7588624974538,23.8518196290644,-48.9609393638615));
#18538=CARTESIAN_POINT('Ctrl Pts',(-26.7586982259238,23.8535623630601,-48.9610481914545));
#18539=CARTESIAN_POINT('Ctrl Pts',(-26.7583519296886,23.8572044099883,-48.9612754713449));
#18540=CARTESIAN_POINT('Ctrl Pts',(-26.7581696380846,23.8591036957877,-48.9613939080884));
#18541=CARTESIAN_POINT('Ctrl Pts',(-26.7577638594909,23.8632923626147,-48.9616549173684));
#18542=CARTESIAN_POINT('Ctrl Pts',(-26.7575396075129,23.8655816725151,-48.961797446419));
#18543=CARTESIAN_POINT('Ctrl Pts',(-26.7567469557411,23.8735852502377,-48.9622953056613));
#18544=CARTESIAN_POINT('Ctrl Pts',(-26.7561657298866,23.8792982810752,-48.9626499128697));
#18545=CARTESIAN_POINT('Ctrl Pts',(-26.7501011337481,23.9373670798313,-48.9662466883265));
#18546=CARTESIAN_POINT('Ctrl Pts',(-26.7433506170332,23.989586292889,-48.9694187468367));
#18547=CARTESIAN_POINT('Ctrl Pts',(-26.734702399696,24.0456444778887,-48.972779159396));
#18548=CARTESIAN_POINT('Ctrl Pts',(-26.734073947508,24.0496675241411,-48.9730200712531));
#18549=CARTESIAN_POINT('Ctrl Pts',(-26.7327533780536,24.0580173644067,-48.9735195850712));
#18550=CARTESIAN_POINT('Ctrl Pts',(-26.7320600572377,24.0623439621837,-48.9737781372859));
#18551=CARTESIAN_POINT('Ctrl Pts',(-26.727678888223,24.0893317850814,-48.9753892327602));
#18552=CARTESIAN_POINT('Ctrl Pts',(-26.7237577079695,24.1119549767869,-48.9767324504512));
#18553=CARTESIAN_POINT('Ctrl Pts',(-26.7172868662011,24.1470549849147,-48.9788077094251));
#18554=CARTESIAN_POINT('Ctrl Pts',(-26.7149045271264,24.1595614837528,-48.9795454113565));
#18555=CARTESIAN_POINT('Ctrl Pts',(-26.6560804733714,24.4587136573785,-48.9971563453131));
#18556=CARTESIAN_POINT('Ctrl Pts',(-26.5609967222382,24.7363857581216,-49.0128667683592));
#18557=CARTESIAN_POINT('Ctrl Pts',(-26.3927833667704,25.0710831774834,-49.0344844041002));
#18558=CARTESIAN_POINT('Ctrl Pts',(-26.3529731138757,25.1432569650069,-49.0393126003399));
#18559=CARTESIAN_POINT('Ctrl Pts',(-26.2884028590074,25.2503917818587,-49.0467899573306));
#18560=CARTESIAN_POINT('Ctrl Pts',(-26.2656385910068,25.2865183429035,-49.0493673024379));
#18561=CARTESIAN_POINT('Ctrl Pts',(-26.2379826302175,25.3285332518099,-49.0524353318259));
#18562=CARTESIAN_POINT('Ctrl Pts',(-26.2337786869781,25.3348709150991,-49.0529000466538));
#18563=CARTESIAN_POINT('Ctrl Pts',(-26.2272991732058,25.344564455887,-49.0536138133581));
#18564=CARTESIAN_POINT('Ctrl Pts',(-26.2250396171451,25.3479310483918,-49.053862260045));
#18565=CARTESIAN_POINT('Ctrl Pts',(-26.2209054998537,25.3540655656761,-49.0543159884572));
#18566=CARTESIAN_POINT('Ctrl Pts',(-26.2190329710048,25.3568348587752,-49.0545211929664));
#18567=CARTESIAN_POINT('Ctrl Pts',(-26.2152578508239,25.3623992265932,-49.0549342774717));
#18568=CARTESIAN_POINT('Ctrl Pts',(-26.2133551629919,25.3651942304437,-49.0551421609653));
#18569=CARTESIAN_POINT('Ctrl Pts',(-26.2079228080447,25.3731472979787,-49.0557347989312));
#18570=CARTESIAN_POINT('Ctrl Pts',(-26.2043825437837,25.3782980740122,-49.0561199567438));
#18571=CARTESIAN_POINT('Ctrl Pts',(-26.1892462226009,25.4001834432565,-49.0577622092377));
#18572=CARTESIAN_POINT('Ctrl Pts',(-26.1775069087434,25.4168179567027,-49.0590247772945));
#18573=CARTESIAN_POINT('Ctrl Pts',(-25.9521505927985,25.7298079857328,-49.0830581709015));
#18574=CARTESIAN_POINT('Ctrl Pts',(-25.6898642055569,25.9877693983333,-49.1080665703639));
#18575=CARTESIAN_POINT('Ctrl Pts',(-25.3309421236721,26.2373426121892,-49.1373663979367));
#18576=CARTESIAN_POINT('Ctrl Pts',(-25.2704222479836,26.2764817802581,-49.1421502015224));
#18577=CARTESIAN_POINT('Ctrl Pts',(-25.1787967277514,26.3314703565341,-49.1491132973499));
#18578=CARTESIAN_POINT('Ctrl Pts',(-25.1486661158156,26.3488955983873,-49.1513599344601));
#18579=CARTESIAN_POINT('Ctrl Pts',(-25.1029056874575,26.374379746724,-49.154701072346));
#18580=CARTESIAN_POINT('Ctrl Pts',(-25.0874834453558,26.3828039431672,-49.1558152027539));
#18581=CARTESIAN_POINT('Ctrl Pts',(-25.06558813087,26.394532470835,-49.1573793834898));
#18582=CARTESIAN_POINT('Ctrl Pts',(-25.0591719272884,26.3979415263556,-49.1578356347659));
#18583=CARTESIAN_POINT('Ctrl Pts',(-25.0479339989977,26.4038638136734,-49.1586309887028));
#18584=CARTESIAN_POINT('Ctrl Pts',(-25.0431173708502,26.4063865795262,-49.158970676795));
#18585=CARTESIAN_POINT('Ctrl Pts',(-25.0360837231905,26.4100478816885,-49.1594649384184));
#18586=CARTESIAN_POINT('Ctrl Pts',(-25.0338717639853,26.411196038153,-49.1596201190301));
#18587=CARTESIAN_POINT('Ctrl Pts',(-25.0300801006743,26.4131585880015,-49.1598856829612));
#18588=CARTESIAN_POINT('Ctrl Pts',(-25.028501053168,26.4139742412838,-49.1599961467792));
#18589=CARTESIAN_POINT('Ctrl Pts',(-25.0253561188513,26.4155954554208,-49.1602158921002));
#18590=CARTESIAN_POINT('Ctrl Pts',(-25.0237902488112,26.4164010379067,-49.1603251749774));
#18591=CARTESIAN_POINT('Ctrl Pts',(-25.0200839518579,26.4183039510962,-49.1605835365493));
#18592=CARTESIAN_POINT('Ctrl Pts',(-25.0179429515142,26.4194001716199,-49.160732544462));
#18593=CARTESIAN_POINT('Ctrl Pts',(-25.0115678307858,26.4226553146899,-49.1611755319071));
#18594=CARTESIAN_POINT('Ctrl Pts',(-25.0073301358853,26.4248072810717,-49.1614690732155));
#18595=CARTESIAN_POINT('Ctrl Pts',(-24.968499562134,26.444418110747,-49.1641505346628));
#18596=CARTESIAN_POINT('Ctrl Pts',(-24.9335973293514,26.4612620708883,-49.1665005369411));
#18597=CARTESIAN_POINT('Ctrl Pts',(-24.8649818034231,26.4928632757829,-49.1710205080573));
#18598=CARTESIAN_POINT('Ctrl Pts',(-24.8313032308686,26.5076805320263,-49.1731932180098));
#18599=CARTESIAN_POINT('Ctrl Pts',(-24.661626097081,26.5788892440546,-49.1839475645431));
#18600=CARTESIAN_POINT('Ctrl Pts',(-24.5221197254395,26.626495791773,-49.1921850125021));
#18601=CARTESIAN_POINT('Ctrl Pts',(-24.3634380166207,26.6687673956451,-49.2013629226141));
#18602=CARTESIAN_POINT('Ctrl Pts',(-24.3470043168155,26.6730064737956,-49.2023110958707));
#18603=CARTESIAN_POINT('Ctrl Pts',(-24.3116216291841,26.6818359598224,-49.2043487884643));
#18604=CARTESIAN_POINT('Ctrl Pts',(-24.2926629426245,26.6863846159111,-49.2054383061194));
#18605=CARTESIAN_POINT('Ctrl Pts',(-24.2514988423938,26.6958667078181,-49.2078007051296));
#18606=CARTESIAN_POINT('Ctrl Pts',(-24.2292801607809,26.7007376378881,-49.2090738141181));
#18607=CARTESIAN_POINT('Ctrl Pts',(-24.1804381771634,26.7109044222156,-49.2118707400491));
#18608=CARTESIAN_POINT('Ctrl Pts',(-24.153795872133,26.7160999277049,-49.2133953263303));
#18609=CARTESIAN_POINT('Ctrl Pts',(-24.0940075435168,26.7269770731785,-49.2168187295836));
#18610=CARTESIAN_POINT('Ctrl Pts',(-24.0608320531575,26.7324776677728,-49.2187197355504));
#18611=CARTESIAN_POINT('Ctrl Pts',(-23.9096143433815,26.755124439188,-49.2274070574949));
#18612=CARTESIAN_POINT('Ctrl Pts',(-23.7907726261889,26.7662268315229,-49.2343005819276));
#18613=CARTESIAN_POINT('Ctrl Pts',(-23.6199393809664,26.7726636754038,-49.244474280415));
#18614=CARTESIAN_POINT('Ctrl Pts',(-23.5682450903625,26.773366807634,-49.2475866494336));
#18615=CARTESIAN_POINT('Ctrl Pts',(-23.5085617023303,26.7727427786152,-49.2512260637711));
#18616=CARTESIAN_POINT('Ctrl Pts',(-23.5005653954728,26.7726294034196,-49.2517146182971));
#18617=CARTESIAN_POINT('Ctrl Pts',(-23.4884328885317,26.7724122131031,-49.2524573533995));
#18618=CARTESIAN_POINT('Ctrl Pts',(-23.4842962890748,26.7723301928601,-49.2527108493687));
#18619=CARTESIAN_POINT('Ctrl Pts',(-23.4768127957714,26.7721673933757,-49.2531699202211));
#18620=CARTESIAN_POINT('Ctrl Pts',(-23.4734658428679,26.7720893641579,-49.2533754084496));
#18621=CARTESIAN_POINT('Ctrl Pts',(-23.4667866720461,26.7719232355739,-49.2537858243134));
#18622=CARTESIAN_POINT('Ctrl Pts',(-23.4634544569821,26.7718351812716,-49.2539907502867));
#18623=CARTESIAN_POINT('Ctrl Pts',(-23.4541116813719,26.7715737911078,-49.2545657987274));
#18624=CARTESIAN_POINT('Ctrl Pts',(-23.4481014836733,26.7713888035794,-49.254936286761));
#18625=CARTESIAN_POINT('Ctrl Pts',(-23.4236315623909,26.7705670908518,-49.2564469980195));
#18626=CARTESIAN_POINT('Ctrl Pts',(-23.4051772417756,26.769788502479,-49.257591668744));
#18627=CARTESIAN_POINT('Ctrl Pts',(-23.0828687255674,26.753413550024,-49.2776798272868));
#18628=CARTESIAN_POINT('Ctrl Pts',(-22.7827898024326,26.6950260697744,-49.2981007390121));
#18629=CARTESIAN_POINT('Ctrl Pts',(-22.4002677386943,26.5625266408897,-49.3254915867263));
#18630=CARTESIAN_POINT('Ctrl Pts',(-22.3066967989176,26.5251191299678,-49.3322869313917));
#18631=CARTESIAN_POINT('Ctrl Pts',(-22.1678264692362,26.4619024759629,-49.3423892443644));
#18632=CARTESIAN_POINT('Ctrl Pts',(-22.1211488588169,26.4392783731394,-49.345787528242));
#18633=CARTESIAN_POINT('Ctrl Pts',(-22.0750360150599,26.4155367744089,-49.3491334787091));
#18634=CARTESIAN_POINT('Ctrl Pts',(-22.0750360207194,26.4155367773228,-49.5934531403533));
#18635=CARTESIAN_POINT('Ctrl Pts',(-22.0975079081856,26.427106624005,-49.5917479670868));
#18636=CARTESIAN_POINT('Ctrl Pts',(-22.1201220559539,26.4384152736554,-49.5900394829616));
#18637=CARTESIAN_POINT('Ctrl Pts',(-22.2880781858102,26.5199471563108,-49.5774121407802));
#18638=CARTESIAN_POINT('Ctrl Pts',(-22.4383791123868,26.5794294445297,-49.5664362692498));
#18639=CARTESIAN_POINT('Ctrl Pts',(-22.642195859053,26.6428660639966,-49.5524125383963));
#18640=CARTESIAN_POINT('Ctrl Pts',(-22.6922520479763,26.657125755106,-49.5490355965523));
#18641=CARTESIAN_POINT('Ctrl Pts',(-22.7675842448179,26.676626167679,-49.5440748684636));
#18642=CARTESIAN_POINT('Ctrl Pts',(-22.792611447065,26.6827853485506,-49.5424465948504));
#18643=CARTESIAN_POINT('Ctrl Pts',(-22.8219311134469,26.6896289436143,-49.5405642764711));
#18644=CARTESIAN_POINT('Ctrl Pts',(-22.8261534477659,26.690605515226,-49.5402938120567));
#18645=CARTESIAN_POINT('Ctrl Pts',(-22.8325981505533,26.6920824030801,-49.5398819344156));
#18646=CARTESIAN_POINT('Ctrl Pts',(-22.8348190797115,26.6925888802357,-49.5397401664924));
#18647=CARTESIAN_POINT('Ctrl Pts',(-22.8386824455193,26.6934656026781,-49.5394938561264));
#18648=CARTESIAN_POINT('Ctrl Pts',(-22.8403246311321,26.6938369147179,-49.5393892518762));
#18649=CARTESIAN_POINT('Ctrl Pts',(-22.843769508272,26.6946129934734,-49.5391700166708));
#18650=CARTESIAN_POINT('Ctrl Pts',(-22.8455722517542,26.69501749574,-49.5390554013944));
#18651=CARTESIAN_POINT('Ctrl Pts',(-22.8500327404483,26.6960143187445,-49.5387720885838));
#18652=CARTESIAN_POINT('Ctrl Pts',(-22.8526908965577,26.6966048231953,-49.538603496288));
#18653=CARTESIAN_POINT('Ctrl Pts',(-22.8631944171482,26.6989241957844,-49.5379382651893));
#18654=CARTESIAN_POINT('Ctrl Pts',(-22.8710455734795,26.7006271145302,-49.5374431113115));
#18655=CARTESIAN_POINT('Ctrl Pts',(-23.0129226856056,26.7308452812935,-49.5285316544743));
#18656=CARTESIAN_POINT('Ctrl Pts',(-23.1486460554971,26.750817537752,-49.5205906024215));
#18657=CARTESIAN_POINT('Ctrl Pts',(-23.3341350994132,26.7661221248341,-49.5100312447018));
#18658=CARTESIAN_POINT('Ctrl Pts',(-23.3831109539556,26.7690392380872,-49.5072709721861));
#18659=CARTESIAN_POINT('Ctrl Pts',(-23.6010741383817,26.7770332020473,-49.4950424786369));
#18660=CARTESIAN_POINT('Ctrl Pts',(-23.7702332011132,26.7699269078915,-49.4856859237203));
#18661=CARTESIAN_POINT('Ctrl Pts',(-24.0436685827172,26.7367830690584,-49.4699576292959));
#18662=CARTESIAN_POINT('Ctrl Pts',(-24.1485773604565,26.7187601420243,-49.4637787988912));
#18663=CARTESIAN_POINT('Ctrl Pts',(-24.2996215711956,26.6850419921105,-49.4545538159176));
#18664=CARTESIAN_POINT('Ctrl Pts',(-24.346601238612,26.6734379680743,-49.451637794015));
#18665=CARTESIAN_POINT('Ctrl Pts',(-24.4008902413153,26.6587240037998,-49.4482077133876));
#18666=CARTESIAN_POINT('Ctrl Pts',(-24.4084728522287,26.6566390636018,-49.4477272534286));
#18667=CARTESIAN_POINT('Ctrl Pts',(-24.4199514200567,26.6534376422684,-49.4469978189516));
#18668=CARTESIAN_POINT('Ctrl Pts',(-24.4238530652423,26.6523415204976,-49.446749508314));
#18669=CARTESIAN_POINT('Ctrl Pts',(-24.4309112744391,26.6503442266845,-49.4462996304829));
#18670=CARTESIAN_POINT('Ctrl Pts',(-24.4340685536346,26.64944558437,-49.4460981461018));
#18671=CARTESIAN_POINT('Ctrl Pts',(-24.4404137991494,26.6476290806542,-49.4456927240257));
#18672=CARTESIAN_POINT('Ctrl Pts',(-24.4436017320988,26.6467111175841,-49.445488783212));
#18673=CARTESIAN_POINT('Ctrl Pts',(-24.4522649111747,26.6442020690492,-49.4449338886527));
#18674=CARTESIAN_POINT('Ctrl Pts',(-24.4577373422873,26.6426013784949,-49.44458262105));
#18675=CARTESIAN_POINT('Ctrl Pts',(-24.4795365833807,26.636162233802,-49.4431803565251));
#18676=CARTESIAN_POINT('Ctrl Pts',(-24.4958289491037,26.6312089999372,-49.4421256045996));
#18677=CARTESIAN_POINT('Ctrl Pts',(-24.7763606749729,26.5434864936577,-49.4238457264704));
#18678=CARTESIAN_POINT('Ctrl Pts',(-25.0288285932198,26.4271494220938,-49.4054204557959));
#18679=CARTESIAN_POINT('Ctrl Pts',(-25.329317273431,26.2385841062258,-49.3814106331462));
#18680=CARTESIAN_POINT('Ctrl Pts',(-25.3938414146064,26.194752173251,-49.3761274987378));
#18681=CARTESIAN_POINT('Ctrl Pts',(-25.5407256476909,26.0869811624334,-49.3638774327463));
#18682=CARTESIAN_POINT('Ctrl Pts',(-25.6217070904627,26.0212958606118,-49.3569477740287));
#18683=CARTESIAN_POINT('Ctrl Pts',(-25.7207034237206,25.9327050749023,-49.3483803895977));
#18684=CARTESIAN_POINT('Ctrl Pts',(-25.7417829977435,25.9133292424876,-49.3465503087621));
#18685=CARTESIAN_POINT('Ctrl Pts',(-25.774103771486,25.8828162298911,-49.3437390337215));
#18686=CARTESIAN_POINT('Ctrl Pts',(-25.7855253558886,25.871873338103,-49.3427445342516));
#18687=CARTESIAN_POINT('Ctrl Pts',(-25.7995523653758,25.8582347365101,-49.3415224050741));
#18688=CARTESIAN_POINT('Ctrl Pts',(-25.8022340037898,25.8556182400417,-49.3412887272013));
#18689=CARTESIAN_POINT('Ctrl Pts',(-25.8064476373062,25.8514925957241,-49.3409215049628));
#18690=CARTESIAN_POINT('Ctrl Pts',(-25.8079826843344,25.8499865912776,-49.3407877144075));
#18691=CARTESIAN_POINT('Ctrl Pts',(-25.8108474325151,25.8471704103993,-49.3405380145509));
#18692=CARTESIAN_POINT('Ctrl Pts',(-25.8121774938252,25.8458606238669,-49.340422076228));
#18693=CARTESIAN_POINT('Ctrl Pts',(-25.8151588621376,25.8429195952922,-49.3401621824195));
#18694=CARTESIAN_POINT('Ctrl Pts',(-25.8168095416713,25.8412877280205,-49.340018277756));
#18695=CARTESIAN_POINT('Ctrl Pts',(-25.8209966632281,25.837139371436,-49.3396532171404));
#18696=CARTESIAN_POINT('Ctrl Pts',(-25.8235306934871,25.8346204372816,-49.3394322545307));
#18697=CARTESIAN_POINT('Ctrl Pts',(-25.8374205879948,25.8207672891992,-49.3382208850104));
#18698=CARTESIAN_POINT('Ctrl Pts',(-25.8486961430384,25.8093523463161,-49.3372367926405));
#18699=CARTESIAN_POINT('Ctrl Pts',(-26.0754332320842,25.5763574069595,-49.3174210730235));
#18700=CARTESIAN_POINT('Ctrl Pts',(-26.2580384844972,25.3249660200484,-49.3008524065526));
#18701=CARTESIAN_POINT('Ctrl Pts',(-26.4897473261149,24.8847689247677,-49.2727421470666));
#18702=CARTESIAN_POINT('Ctrl Pts',(-26.5626610031226,24.7108310567506,-49.2618486030793));
#18703=CARTESIAN_POINT('Ctrl Pts',(-26.6229904198606,24.5221051770588,-49.2497845587341));
#18704=CARTESIAN_POINT('Ctrl Pts',(-26.6259631645772,24.5126556660406,-49.2491799745773));
#18705=CARTESIAN_POINT('Ctrl Pts',(-26.630227447683,24.4988791540285,-49.2482977158869));
#18706=CARTESIAN_POINT('Ctrl Pts',(-26.6315535536646,24.4945628426601,-49.2480211775141));
#18707=CARTESIAN_POINT('Ctrl Pts',(-26.6338606809879,24.486996822905,-49.2475362235022));
#18708=CARTESIAN_POINT('Ctrl Pts',(-26.6348456496207,24.4837483175464,-49.2473279377194));
#18709=CARTESIAN_POINT('Ctrl Pts',(-26.6367450352745,24.4774481618576,-49.2469238527489));
#18710=CARTESIAN_POINT('Ctrl Pts',(-26.6376600638998,24.474396698591,-49.2467280738751));
#18711=CARTESIAN_POINT('Ctrl Pts',(-26.6398287843243,24.4671252175234,-49.2462613942141));
#18712=CARTESIAN_POINT('Ctrl Pts',(-26.6410783544322,24.4629039854447,-49.2459903587622));
#18713=CARTESIAN_POINT('Ctrl Pts',(-26.6454910646547,24.4478841939649,-49.2450255407615));
#18714=CARTESIAN_POINT('Ctrl Pts',(-26.6486062662182,24.4370717396631,-49.2443301930727));
#18715=CARTESIAN_POINT('Ctrl Pts',(-26.6936083217375,24.2777436628749,-49.2340715857434));
#18716=CARTESIAN_POINT('Ctrl Pts',(-26.7248259381615,24.1264468228135,-49.2241588555701));
#18717=CARTESIAN_POINT('Ctrl Pts',(-26.7500987126622,23.9356850347559,-49.2114473536258));
#18718=CARTESIAN_POINT('Ctrl Pts',(-26.754438131268,23.8977698691747,-49.208911385436));
#18719=CARTESIAN_POINT('Ctrl Pts',(-26.7681229096629,23.755948325642,-49.1993965020762));
#18720=CARTESIAN_POINT('Ctrl Pts',(-26.7730944442293,23.6516874405683,-49.1923409029875));
#18721=CARTESIAN_POINT('Ctrl Pts',(-26.7728465732488,23.3742538390487,-49.1735607967991));
#18722=CARTESIAN_POINT('Ctrl Pts',(-26.7587427175285,23.2014123261941,-49.1618456192302));
#18723=CARTESIAN_POINT('Ctrl Pts',(-26.7245902886662,22.9924091793172,-49.1482161848915));
#18724=CARTESIAN_POINT('Ctrl Pts',(-26.7176763179749,22.9544033133532,-49.1457606099963));
#18725=CARTESIAN_POINT('Ctrl Pts',(-26.7091465976908,22.9118730275633,-49.1430453772746));
#18726=CARTESIAN_POINT('Ctrl Pts',(-26.7082025381722,22.9072191976012,-49.1427487073633));
#18727=CARTESIAN_POINT('Ctrl Pts',(-26.7067649862634,22.900212173412,-49.1423027101931));
#18728=CARTESIAN_POINT('Ctrl Pts',(-26.7062791461965,22.897857442893,-49.1421529478476));
#18729=CARTESIAN_POINT('Ctrl Pts',(-26.7054329484205,22.893779226352,-49.1418937748276));
#18730=CARTESIAN_POINT('Ctrl Pts',(-26.7050738134907,22.8920554922917,-49.1417842937381));
#18731=CARTESIAN_POINT('Ctrl Pts',(-26.7043223835432,22.8884636106587,-49.1415562922983));
#18732=CARTESIAN_POINT('Ctrl Pts',(-26.7039298417775,22.8865955192,-49.1414377868705));
#18733=CARTESIAN_POINT('Ctrl Pts',(-26.702992768437,22.8821556279684,-49.1411563117007));
#18734=CARTESIAN_POINT('Ctrl Pts',(-26.7024467478438,22.8795841360348,-49.140993428033));
#18735=CARTESIAN_POINT('Ctrl Pts',(-26.7006120045458,22.8709951242968,-49.14044984406));
#18736=CARTESIAN_POINT('Ctrl Pts',(-26.6993091821647,22.8649805803513,-49.140069951718));
#18737=CARTESIAN_POINT('Ctrl Pts',(-26.662882204658,22.6991113693642,-49.1296132755312));
#18738=CARTESIAN_POINT('Ctrl Pts',(-26.6156426434075,22.5421329476644,-49.1202253442559));
#18739=CARTESIAN_POINT('Ctrl Pts',(-26.4668300842655,22.1567317040386,-49.0969464905421));
#18740=CARTESIAN_POINT('Ctrl Pts',(-26.3502907431995,21.9352887576804,-49.0832904496715));
#18741=CARTESIAN_POINT('Ctrl Pts',(-26.1551382330422,21.6502770974722,-49.0631597745355));
#18742=CARTESIAN_POINT('Ctrl Pts',(-26.0973851441392,21.5735257343748,-49.0574548132892));
#18743=CARTESIAN_POINT('Ctrl Pts',(-26.0298197343569,21.4916200614403,-49.0509917225545));
#18744=CARTESIAN_POINT('Ctrl Pts',(-26.023305729356,21.4837992808552,-49.0503706669106));
#18745=CARTESIAN_POINT('Ctrl Pts',(-26.0140654140519,21.4728115328613,-49.0494925069135));
#18746=CARTESIAN_POINT('Ctrl Pts',(-26.0113697775207,21.4696187520656,-49.0492366610302));
#18747=CARTESIAN_POINT('Ctrl Pts',(-26.0066449951567,21.4640446283018,-49.0487888083604));
#18748=CARTESIAN_POINT('Ctrl Pts',(-26.0046185722838,21.4616609753031,-49.0485969138496));
#18749=CARTESIAN_POINT('Ctrl Pts',(-26.0003592561216,21.4566655598788,-49.0481939605298));
#18750=CARTESIAN_POINT('Ctrl Pts',(-25.9981256517518,21.4540544118602,-49.0479828724923));
#18751=CARTESIAN_POINT('Ctrl Pts',(-25.9927911105632,21.4478383325835,-49.0474792550143));
#18752=CARTESIAN_POINT('Ctrl Pts',(-25.9896863693835,21.4442366901025,-49.0471865680764));
#18753=CARTESIAN_POINT('Ctrl Pts',(-25.9792148496023,21.4321434700043,-49.0462008131347));
#18754=CARTESIAN_POINT('Ctrl Pts',(-25.9718116768996,21.4236836425772,-49.0455062308958));
#18755=CARTESIAN_POINT('Ctrl Pts',(-25.954237683648,21.403812077674,-49.043862769157));
#18756=CARTESIAN_POINT('Ctrl Pts',(-25.9440297011954,21.3924337062935,-49.0429123343568));
#18757=CARTESIAN_POINT('Ctrl Pts',(-25.828747511873,21.2657586962357,-49.0322243092749));
#18758=CARTESIAN_POINT('Ctrl Pts',(-25.7155322675603,21.158181840617,-49.0221323626888));
#18759=CARTESIAN_POINT('Ctrl Pts',(-25.3442072907263,20.853381890382,-48.9902367271506));
#18760=CARTESIAN_POINT('Ctrl Pts',(-25.0637981232711,20.6865913387992,-48.9675634603602));
#18761=CARTESIAN_POINT('Ctrl Pts',(-24.7628766840616,20.5643422241424,-48.9470143995007));
#18762=CARTESIAN_POINT('Ctrl Pts',(-24.7625335605392,20.5642028993626,-48.9469909734531));
#18763=CARTESIAN_POINT('Ctrl Pts',(-24.7478156332019,20.5582296624775,-48.9459863466688));
#18764=CARTESIAN_POINT('Ctrl Pts',(-24.7333985690961,20.5524994215711,-48.9450108147615));
#18765=CARTESIAN_POINT('Ctrl Pts',(-24.7156503350406,20.5455931523956,-48.9438208531043));
#18766=CARTESIAN_POINT('Ctrl Pts',(-24.7123582021844,20.5443183280629,-48.9436005878669));
#18767=CARTESIAN_POINT('Ctrl Pts',(-24.7069104785225,20.5422190739908,-48.9432368703767));
#18768=CARTESIAN_POINT('Ctrl Pts',(-24.7047560966887,20.5413915500088,-48.9430932320644));
#18769=CARTESIAN_POINT('Ctrl Pts',(-24.7009722156792,20.5399427781028,-48.9428413024894));
#18770=CARTESIAN_POINT('Ctrl Pts',(-24.6993431046424,20.5393205399532,-48.9427329512655));
#18771=CARTESIAN_POINT('Ctrl Pts',(-24.6960077625151,20.5380497089426,-48.9425113541662));
#18772=CARTESIAN_POINT('Ctrl Pts',(-24.6943014910657,20.5374012454627,-48.942398116341));
#18773=CARTESIAN_POINT('Ctrl Pts',(-24.6895891676365,20.5356149210458,-48.9420857233108));
#18774=CARTESIAN_POINT('Ctrl Pts',(-24.6865819524212,20.5344801030549,-48.9418867521956));
#18775=CARTESIAN_POINT('Ctrl Pts',(-24.6800165066005,20.5320137476784,-48.9414531826345));
#18776=CARTESIAN_POINT('Ctrl Pts',(-24.6764576031618,20.5306839973368,-48.9412186907904));
#18777=CARTESIAN_POINT('Ctrl Pts',(-24.6660756237772,20.5268257776988,-48.9405361597888));
#18778=CARTESIAN_POINT('Ctrl Pts',(-24.6592462709372,20.5243140990271,-48.9400891028638));
#18779=CARTESIAN_POINT('Ctrl Pts',(-24.5883057218364,20.4984962264614,-48.9354645519725));
#18780=CARTESIAN_POINT('Ctrl Pts',(-24.5234730010526,20.4772060860717,-48.9314013395652));
#18781=CARTESIAN_POINT('Ctrl Pts',(-24.4157737530889,20.4455902263549,-48.9248424599982));
#18782=CARTESIAN_POINT('Ctrl Pts',(-24.3732883040271,20.434058151931,-48.9223029286349));
#18783=CARTESIAN_POINT('Ctrl Pts',(-24.0470997403555,20.3526557288685,-48.9030783291185));
#18784=CARTESIAN_POINT('Ctrl Pts',(-23.755322356125,20.3207878374269,-48.8873132788591));
#18785=CARTESIAN_POINT('Ctrl Pts',(-23.3648675914253,20.3313345686431,-48.8645729784289));
#18786=CARTESIAN_POINT('Ctrl Pts',(-23.2666840494428,20.3384950137551,-48.8587301292027));
#18787=CARTESIAN_POINT('Ctrl Pts',(-23.1597143991977,20.3512394398913,-48.852173053691));
#18788=CARTESIAN_POINT('Ctrl Pts',(-23.1504451083214,20.3523846770462,-48.8516032989546));
#18789=CARTESIAN_POINT('Ctrl Pts',(-23.1366942888761,20.3541443353795,-48.8507557163725));
#18790=CARTESIAN_POINT('Ctrl Pts',(-23.1322088070671,20.3547279320841,-48.8504788636787));
#18791=CARTESIAN_POINT('Ctrl Pts',(-23.1245343506585,20.3557428747286,-48.8500045366332));
#18792=CARTESIAN_POINT('Ctrl Pts',(-23.121344756971,20.356169558636,-48.8498072100856));
#18793=CARTESIAN_POINT('Ctrl Pts',(-23.1151424394857,20.3570087237739,-48.8494231261229));
#18794=CARTESIAN_POINT('Ctrl Pts',(-23.1121296494338,20.3574206931681,-48.849236385148));
#18795=CARTESIAN_POINT('Ctrl Pts',(-23.10492770969,20.3584158731929,-48.8487895774475));
#18796=CARTESIAN_POINT('Ctrl Pts',(-23.1007391244065,20.3590030666663,-48.8485293847339));
#18797=CARTESIAN_POINT('Ctrl Pts',(-23.088193334579,20.3607870378944,-48.8477490412913));
#18798=CARTESIAN_POINT('Ctrl Pts',(-23.0798397131253,20.362008404321,-48.8472281114063));
#18799=CARTESIAN_POINT('Ctrl Pts',(-23.0071060890651,20.3729347197549,-48.8426806507235));
#18800=CARTESIAN_POINT('Ctrl Pts',(-22.9430331663998,20.3845551079751,-48.8385935403762));
#18801=CARTESIAN_POINT('Ctrl Pts',(-22.7795942385087,20.4193409439302,-48.8279471217776));
#18802=CARTESIAN_POINT('Ctrl Pts',(-22.680902384818,20.4452970665587,-48.8213040210221));
#18803=CARTESIAN_POINT('Ctrl Pts',(-22.2927887270105,20.5673271822396,-48.7943588920547));
#18804=CARTESIAN_POINT('Ctrl Pts',(-22.0164366043374,20.6995595218724,-48.7731376931124));
#18805=CARTESIAN_POINT('Ctrl Pts',(-21.7590763505427,20.8711061508532,-48.7531965094375));
#18806=CARTESIAN_POINT('Ctrl Pts',(-21.7553714803239,20.8735867972799,-48.7529094398673));
#18807=CARTESIAN_POINT('Ctrl Pts',(-21.7208600317703,20.8967982821713,-48.7502353989753));
#18808=CARTESIAN_POINT('Ctrl Pts',(-21.6904070868979,20.9180535288288,-48.7478762290566));
#18809=CARTESIAN_POINT('Ctrl Pts',(-21.6561563794648,20.9428507911263,-48.7452295622994));
#18810=CARTESIAN_POINT('Ctrl Pts',(-21.6519932286792,20.945880114009,-48.7449079767908));
#18811=CARTESIAN_POINT('Ctrl Pts',(-21.6458566494886,20.9503679366434,-48.7444341446921));
#18812=CARTESIAN_POINT('Ctrl Pts',(-21.6438776249272,20.9518187152021,-48.744281365186));
#18813=CARTESIAN_POINT('Ctrl Pts',(-21.6403797496466,20.9543890762678,-48.7440113866434));
#18814=CARTESIAN_POINT('Ctrl Pts',(-21.6388602241925,20.9555077331211,-48.7438941228026));
#18815=CARTESIAN_POINT('Ctrl Pts',(-21.6357252400114,20.9578199200212,-48.7436522312593));
#18816=CARTESIAN_POINT('Ctrl Pts',(-21.6341099180439,20.9590136232046,-48.7435276163908));
#18817=CARTESIAN_POINT('Ctrl Pts',(-21.629933555164,20.9621059449428,-48.7432054810465));
#18818=CARTESIAN_POINT('Ctrl Pts',(-21.6273742057868,20.9640068608231,-48.743008121826));
#18819=CARTESIAN_POINT('Ctrl Pts',(-21.6218016326251,20.9681586453014,-48.7425785049554));
#18820=CARTESIAN_POINT('Ctrl Pts',(-21.6187895150299,20.9704110009285,-48.7423463507975));
#18821=CARTESIAN_POINT('Ctrl Pts',(-21.6100418219927,20.9769761258533,-48.7416723023923));
#18822=CARTESIAN_POINT('Ctrl Pts',(-21.60431665445,20.9813028196859,-48.7412313611109));
#18823=CARTESIAN_POINT('Ctrl Pts',(-21.5455872353762,21.0259955195116,-48.7367097339907));
#18824=CARTESIAN_POINT('Ctrl Pts',(-21.4938279911415,21.0679801873633,-48.7327381148028));
#18825=CARTESIAN_POINT('Ctrl Pts',(-21.3627479563389,21.1812227873413,-48.7226056379018));
#18826=CARTESIAN_POINT('Ctrl Pts',(-21.2855929496266,21.2548662223083,-48.7165652180958));
#18827=CARTESIAN_POINT('Ctrl Pts',(-21.0731017897852,21.4788513419078,-48.6992272074093));
#18828=CARTESIAN_POINT('Ctrl Pts',(-20.9480900870268,21.6382570778448,-48.6880825141914));
#18829=CARTESIAN_POINT('Ctrl Pts',(-20.8077338175771,21.85672976859,-48.6731335150186));
#18830=CARTESIAN_POINT('Ctrl Pts',(-20.7779369415227,21.9059611960316,-48.6697866944855));
#18831=CARTESIAN_POINT('Ctrl Pts',(-20.740665065862,21.9714387434569,-48.6653467193498));
#18832=CARTESIAN_POINT('Ctrl Pts',(-20.731983770707,21.9869880373438,-48.6642931713985));
#18833=CARTESIAN_POINT('Ctrl Pts',(-20.7196249112983,22.0095618803614,-48.6627644163005));
#18834=CARTESIAN_POINT('Ctrl Pts',(-20.715843603709,22.0165294680999,-48.6622926563766));
#18835=CARTESIAN_POINT('Ctrl Pts',(-20.7112096620727,22.0251438191769,-48.6617094911271));
#18836=CARTESIAN_POINT('Ctrl Pts',(-20.7103326680423,22.0267775011935,-48.6615988999826));
#18837=CARTESIAN_POINT('Ctrl Pts',(-20.6880236897193,22.0684213134511,-48.6587799436781));
#18838=CARTESIAN_POINT('Ctrl Pts',(-20.6674387997649,22.108877364906,-48.6560435618705));
#18839=CARTESIAN_POINT('Ctrl Pts',(-20.6444612748875,22.1564983122312,-48.6528203313566));
#18840=CARTESIAN_POINT('Ctrl Pts',(-20.6412302114293,22.1632547699389,-48.6523629709846));
#18841=CARTESIAN_POINT('Ctrl Pts',(-20.6361170882535,22.1740432530182,-48.6516325725699));
#18842=CARTESIAN_POINT('Ctrl Pts',(-20.6342197637046,22.1780680480595,-48.6513600649143));
#18843=CARTESIAN_POINT('Ctrl Pts',(-20.6308888814549,22.1851719567128,-48.6508790346522));
#18844=CARTESIAN_POINT('Ctrl Pts',(-20.6294518416437,22.1882494379421,-48.6506706330818));
#18845=CARTESIAN_POINT('Ctrl Pts',(-20.626493778627,22.1946104655199,-48.6502398427367));
#18846=CARTESIAN_POINT('Ctrl Pts',(-20.6249734161483,22.1978943122497,-48.650017431471));
#18847=CARTESIAN_POINT('Ctrl Pts',(-20.6211014698528,22.2062944498116,-48.649448449743));
#18848=CARTESIAN_POINT('Ctrl Pts',(-20.6187577653232,22.2114143401864,-48.6491016077772));
#18849=CARTESIAN_POINT('Ctrl Pts',(-20.6092979203606,22.2322235745123,-48.6476916940024));
#18850=CARTESIAN_POINT('Ctrl Pts',(-20.6022943229896,22.2479634934697,-48.646624756197));
#18851=CARTESIAN_POINT('Ctrl Pts',(-20.557509296215,22.350826293858,-48.6396481040668));
#18852=CARTESIAN_POINT('Ctrl Pts',(-20.5234716410309,22.4395186480559,-48.6336116327341));
#18853=CARTESIAN_POINT('Ctrl Pts',(-20.448169579379,22.6650430433396,-48.6181940329165));
#18854=CARTESIAN_POINT('Ctrl Pts',(-20.4119972063323,22.8033520262698,-48.6086721098018));
#18855=CARTESIAN_POINT('Ctrl Pts',(-20.3377497671372,23.1907227166895,-48.5820633003659));
#18856=CARTESIAN_POINT('Ctrl Pts',(-20.3194846789699,23.4425699382387,-48.5647823129555));
#18857=CARTESIAN_POINT('Ctrl Pts',(-20.3313394823289,23.7080998643683,-48.5479918722126));
#18858=CARTESIAN_POINT('Ctrl Pts',(-20.3320620944576,23.7222040567293,-48.5471045035409));
#18859=CARTESIAN_POINT('Ctrl Pts',(-20.3330934036003,23.7400384765182,-48.5459885177985));
#18860=CARTESIAN_POINT('Ctrl Pts',(-20.333315899882,23.7437732478306,-48.5457551521051));
#18861=CARTESIAN_POINT('Ctrl Pts',(-20.3336778134725,23.7496750984065,-48.5453869190254));
#18862=CARTESIAN_POINT('Ctrl Pts',(-20.3338129172378,23.7518424238998,-48.5452518089594));
#18863=CARTESIAN_POINT('Ctrl Pts',(-20.334065783101,23.7558339074541,-48.5450031964936));
#18864=CARTESIAN_POINT('Ctrl Pts',(-20.3341829058967,23.7576580907777,-48.5448896587522));
#18865=CARTESIAN_POINT('Ctrl Pts',(-20.3344464202711,23.7617084214813,-48.5446377482922));
#18866=CARTESIAN_POINT('Ctrl Pts',(-20.3345935710591,23.7639345116348,-48.544499419321));
#18867=CARTESIAN_POINT('Ctrl Pts',(-20.3349043507566,23.7685629432944,-48.5442120611435));
#18868=CARTESIAN_POINT('Ctrl Pts',(-20.3350683608361,23.7709652590692,-48.5440630535227));
#18869=CARTESIAN_POINT('Ctrl Pts',(-20.3354980941764,23.7771575859987,-48.5436793229908));
#18870=CARTESIAN_POINT('Ctrl Pts',(-20.3357678283208,23.7809473286343,-48.5434448240731));
#18871=CARTESIAN_POINT('Ctrl Pts',(-20.3365737164673,23.7919941015368,-48.5427622673769));
#18872=CARTESIAN_POINT('Ctrl Pts',(-20.3371277526264,23.7992498620811,-48.5423151919203));
#18873=CARTESIAN_POINT('Ctrl Pts',(-20.3391065050481,23.8240568978418,-48.5407907270635));
#18874=CARTESIAN_POINT('Ctrl Pts',(-20.3406505198908,23.8415987047001,-48.5397196866321));
#18875=CARTESIAN_POINT('Ctrl Pts',(-20.3456832336404,23.8938674875193,-48.5365467506839));
#18876=CARTESIAN_POINT('Ctrl Pts',(-20.3495924405204,23.9285524298016,-48.5344654922422));
#18877=CARTESIAN_POINT('Ctrl Pts',(-20.3652006573589,24.049368293463,-48.5272795874743));
#18878=CARTESIAN_POINT('Ctrl Pts',(-20.3798202344228,24.1350885065831,-48.5222938628633));
#18879=CARTESIAN_POINT('Ctrl Pts',(-20.4706944076417,24.5627391530154,-48.4975367452816));
#18880=CARTESIAN_POINT('Ctrl Pts',(-20.5988529322427,24.8911651671507,-48.4785968961045));
#18881=CARTESIAN_POINT('Ctrl Pts',(-20.7876612272928,25.209956255913,-48.4561885134168));
#18882=CARTESIAN_POINT('Ctrl Pts',(-20.7981383384728,25.2272720920309,-48.4549586436408));
#18883=CARTESIAN_POINT('Ctrl Pts',(-20.8120558656314,25.249792312028,-48.4533419952281));
#18884=CARTESIAN_POINT('Ctrl Pts',(-20.8153494342785,25.2550872726168,-48.4529606380494));
#18885=CARTESIAN_POINT('Ctrl Pts',(-20.8204510410486,25.2632361269736,-48.4523717918824));
#18886=CARTESIAN_POINT('Ctrl Pts',(-20.8222482467243,25.2660968128208,-48.4521647044679));
#18887=CARTESIAN_POINT('Ctrl Pts',(-20.8258329671119,25.2717828906178,-48.4517523436892));
#18888=CARTESIAN_POINT('Ctrl Pts',(-20.8276203870326,25.274608337581,-48.4515470740206));
#18889=CARTESIAN_POINT('Ctrl Pts',(-20.8315878686558,25.2808583483926,-48.4510921969015));
#18890=CARTESIAN_POINT('Ctrl Pts',(-20.8337700082759,25.2842815806338,-48.4508425122894));
#18891=CARTESIAN_POINT('Ctrl Pts',(-20.8400710570237,25.2941252692056,-48.4501229653665));
#18892=CARTESIAN_POINT('Ctrl Pts',(-20.8442062802706,25.3005352042462,-48.4496524943695));
#18893=CARTESIAN_POINT('Ctrl Pts',(-20.8718904811528,25.3431153624163,-48.4465143207082));
#18894=CARTESIAN_POINT('Ctrl Pts',(-20.8961403222089,25.3788225989339,-48.443820369126));
#18895=CARTESIAN_POINT('Ctrl Pts',(-20.9681639066834,25.4804232403466,-48.4359681182858));
#18896=CARTESIAN_POINT('Ctrl Pts',(-21.0177230796161,25.5450039781833,-48.4307425078457));
#18897=CARTESIAN_POINT('Ctrl Pts',(-21.1004073196492,25.6446961986292,-48.422291871813));
#18898=CARTESIAN_POINT('Ctrl Pts',(-21.1319705186023,25.681061677452,-48.4191224527582));
#18899=CARTESIAN_POINT('Ctrl Pts',(-21.1889691182188,25.7438343083818,-48.4134997066853));
#18900=CARTESIAN_POINT('Ctrl Pts',(-21.2140631719153,25.7705406954405,-48.4110566128114));
#18901=CARTESIAN_POINT('Ctrl Pts',(-21.4358619832459,25.998666563722,-48.3897529547349));
#18902=CARTESIAN_POINT('Ctrl Pts',(-21.6577186481136,26.173933440987,-48.3702486348577));
#18903=CARTESIAN_POINT('Ctrl Pts',(-21.9053380276005,26.3216095283544,-48.3518747842697));
#18904=CARTESIAN_POINT('Ctrl Pts',(-21.9111592331467,26.3250563966818,-48.3514446649301));
#18905=CARTESIAN_POINT('Ctrl Pts',(-21.9278492457012,26.3348680849572,-48.3502167771492));
#18906=CARTESIAN_POINT('Ctrl Pts',(-21.9387447201346,26.3411876415089,-48.3494216139709));
#18907=CARTESIAN_POINT('Ctrl Pts',(-21.9568727300183,26.3515606366444,-48.348109579425));
#18908=CARTESIAN_POINT('Ctrl Pts',(-21.9640842467949,26.3556502694197,-48.3475904934599));
#18909=CARTESIAN_POINT('Ctrl Pts',(-21.9739852532848,26.3612147221348,-48.3468818062777));
#18910=CARTESIAN_POINT('Ctrl Pts',(-21.9766611051454,26.3627135521442,-48.3466906736602));
#18911=CARTESIAN_POINT('Ctrl Pts',(-21.980910151939,26.3650856164445,-48.3463878051533));
#18912=CARTESIAN_POINT('Ctrl Pts',(-21.9824819369371,26.3659613522498,-48.3462759073395));
#18913=CARTESIAN_POINT('Ctrl Pts',(-21.9856304259121,26.3677121108605,-48.3460520383965));
#18914=CARTESIAN_POINT('Ctrl Pts',(-21.9872071265352,26.3685871242438,-48.3459400683186));
#18915=CARTESIAN_POINT('Ctrl Pts',(-21.9908787648564,26.3706207255406,-48.3456796473428));
#18916=CARTESIAN_POINT('Ctrl Pts',(-21.9929742645306,26.3717783055037,-48.3455312619089));
#18917=CARTESIAN_POINT('Ctrl Pts',(-21.9994071743167,26.375322574951,-48.3450764789039));
#18918=CARTESIAN_POINT('Ctrl Pts',(-22.0037488217754,26.3777016201463,-48.3447705724961));
#18919=CARTESIAN_POINT('Ctrl Pts',(-22.0137691854714,26.3831623843668,-48.3440668874065));
#18920=CARTESIAN_POINT('Ctrl Pts',(-22.0194517439059,26.386237062041,-48.3436695505007));
#18921=CARTESIAN_POINT('Ctrl Pts',(-22.0383482932117,26.3963881254767,-48.342353846686));
#18922=CARTESIAN_POINT('Ctrl Pts',(-22.051602636388,26.4033895342728,-48.3414400290071));
#18923=CARTESIAN_POINT('Ctrl Pts',(-22.0682793503257,26.4120504812494,-48.3403009377785));
#18924=CARTESIAN_POINT('Ctrl Pts',(-22.0716561491687,26.4137966210548,-48.3400708338911));
#18925=CARTESIAN_POINT('Ctrl Pts',(-22.0750360153631,26.415536774565,-48.3398410585546));
#18926=CARTESIAN_POINT('Origin',(-23.5502525316942,23.5502525316942,-77.3107734492734));
#18927=CARTESIAN_POINT('',(-22.0750360041347,26.415536768784,-46.8440307128639));
#18928=CARTESIAN_POINT('',(-22.075036119826,26.4155368283487,-47.0942077761624));
#18929=CARTESIAN_POINT('',(-22.0750360153461,26.4155367745563,-77.3107734492734));
#18930=CARTESIAN_POINT('Ctrl Pts',(-22.0750360041347,26.415536768784,-46.8440307128639));
#18931=CARTESIAN_POINT('Ctrl Pts',(-22.0617973538971,26.4087207344862,-46.8448939685705));
#18932=CARTESIAN_POINT('Ctrl Pts',(-22.0486049166737,26.4018124210467,-46.845759825945));
#18933=CARTESIAN_POINT('Ctrl Pts',(-21.9782325485303,26.364337531751,-46.8504099569758));
#18934=CARTESIAN_POINT('Ctrl Pts',(-21.9219412593692,26.3321444734535,-46.8542415819791));
#18935=CARTESIAN_POINT('Ctrl Pts',(-21.8475121248935,26.2865451003208,-46.8594816902241));
#18936=CARTESIAN_POINT('Ctrl Pts',(-21.8284860184323,26.2746133648144,-46.8608369379362));
#18937=CARTESIAN_POINT('Ctrl Pts',(-21.7968069472908,26.2542822525078,-46.8631208245042));
#18938=CARTESIAN_POINT('Ctrl Pts',(-21.784085668844,26.2459904174565,-46.8640454691496));
#18939=CARTESIAN_POINT('Ctrl Pts',(-21.7669628396108,26.2346563861459,-46.8653004175424));
#18940=CARTESIAN_POINT('Ctrl Pts',(-21.7625094261512,26.2316925865386,-46.8656277691874));
#18941=CARTESIAN_POINT('Ctrl Pts',(-21.7554580687743,26.2269744495097,-46.8661476128196));
#18942=CARTESIAN_POINT('Ctrl Pts',(-21.7528552560251,26.2252273769495,-46.8663398300661));
#18943=CARTESIAN_POINT('Ctrl Pts',(-21.7474601347964,26.2215946080767,-46.8667389491385));
#18944=CARTESIAN_POINT('Ctrl Pts',(-21.744668227357,26.2197083255139,-46.8669458730176));
#18945=CARTESIAN_POINT('Ctrl Pts',(-21.7382840745544,26.2153804345445,-46.8674199227538));
#18946=CARTESIAN_POINT('Ctrl Pts',(-21.7346938025153,26.2129359392415,-46.8676871580563));
#18947=CARTESIAN_POINT('Ctrl Pts',(-21.7236702483595,26.2053977112748,-46.8685096626089));
#18948=CARTESIAN_POINT('Ctrl Pts',(-21.7162534270643,26.2002800870252,-46.8690658416));
#18949=CARTESIAN_POINT('Ctrl Pts',(-21.6606080051764,26.1615391217311,-46.8732597979878));
#18950=CARTESIAN_POINT('Ctrl Pts',(-21.6132888367138,26.1266346848498,-46.8769466360745));
#18951=CARTESIAN_POINT('Ctrl Pts',(-21.5553188563046,26.081373836786,-46.8816212885295));
#18952=CARTESIAN_POINT('Ctrl Pts',(-21.5437472971752,26.0722105334717,-46.8825625199561));
#18953=CARTESIAN_POINT('Ctrl Pts',(-21.4904405882721,26.029398826164,-46.8869363410957));
#18954=CARTESIAN_POINT('Ctrl Pts',(-21.4494880835879,25.9947933490911,-46.8904050929509));
#18955=CARTESIAN_POINT('Ctrl Pts',(-21.2132317707212,25.7848308368318,-46.9110648058796));
#18956=CARTESIAN_POINT('Ctrl Pts',(-21.0390894741094,25.587170814896,-46.9290988687397));
#18957=CARTESIAN_POINT('Ctrl Pts',(-20.8672048519715,25.33606538398,-46.9494424758253));
#18958=CARTESIAN_POINT('Ctrl Pts',(-20.8442181698907,25.3010382588787,-46.9522259833028));
#18959=CARTESIAN_POINT('Ctrl Pts',(-20.7858165773178,25.2081465426222,-46.9594495812359));
#18960=CARTESIAN_POINT('Ctrl Pts',(-20.7515318668456,25.1495907884584,-46.9638467998252));
#18961=CARTESIAN_POINT('Ctrl Pts',(-20.7116783729464,25.0763117731561,-46.9691215314157));
#18962=CARTESIAN_POINT('Ctrl Pts',(-20.7043373737445,25.0625775629877,-46.9701005227528));
#18963=CARTESIAN_POINT('Ctrl Pts',(-20.6953629075255,25.0454905357816,-46.9713061247124));
#18964=CARTESIAN_POINT('Ctrl Pts',(-20.6936354890233,25.0421876934592,-46.9715385917781));
#18965=CARTESIAN_POINT('Ctrl Pts',(-20.690922496168,25.0369784365136,-46.9719043332558));
#18966=CARTESIAN_POINT('Ctrl Pts',(-20.6899330963325,25.0350740347311,-46.97203785059));
#18967=CARTESIAN_POINT('Ctrl Pts',(-20.6880864950052,25.031510992184,-46.9722872968151));
#18968=CARTESIAN_POINT('Ctrl Pts',(-20.687228838393,25.029852606029,-46.9724032541889));
#18969=CARTESIAN_POINT('Ctrl Pts',(-20.6853055385183,25.0261257318557,-46.9726635190122));
#18970=CARTESIAN_POINT('Ctrl Pts',(-20.6842406962814,25.0240568389309,-46.9728077749742));
#18971=CARTESIAN_POINT('Ctrl Pts',(-20.6815379590678,25.0187916568753,-46.9731743301255));
#18972=CARTESIAN_POINT('Ctrl Pts',(-20.6799031598458,25.0155937701784,-46.9733964332031));
#18973=CARTESIAN_POINT('Ctrl Pts',(-20.6708892976152,24.9978884815273,-46.9746232294401));
#18974=CARTESIAN_POINT('Ctrl Pts',(-20.6636146991916,24.9833277311196,-46.9756214188908));
#18975=CARTESIAN_POINT('Ctrl Pts',(-20.5203407810084,24.6910343531535,-46.9954579244464));
#18976=CARTESIAN_POINT('Ctrl Pts',(-20.4248799514166,24.3951600816855,-47.0120341698549));
#18977=CARTESIAN_POINT('Ctrl Pts',(-20.3555298369252,23.9870622586498,-47.0354281403252));
#18978=CARTESIAN_POINT('Ctrl Pts',(-20.3430388509584,23.8831695340491,-47.041413946819));
#18979=CARTESIAN_POINT('Ctrl Pts',(-20.3315873573965,23.7221400975372,-47.0508755450341));
#18980=CARTESIAN_POINT('Ctrl Pts',(-20.3290558537634,23.6653273840794,-47.0542481709916));
#18981=CARTESIAN_POINT('Ctrl Pts',(-20.3276607328868,23.588123216149,-47.0588915530379));
#18982=CARTESIAN_POINT('Ctrl Pts',(-20.3274857990944,23.5677639183115,-47.0601217008978));
#18983=CARTESIAN_POINT('Ctrl Pts',(-20.3275162039612,23.5333564938741,-47.0622108183582));
#18984=CARTESIAN_POINT('Ctrl Pts',(-20.3276204731539,23.5193087169935,-47.0630666177642));
#18985=CARTESIAN_POINT('Ctrl Pts',(-20.3278890102855,23.5000747061631,-47.0642424210385));
#18986=CARTESIAN_POINT('Ctrl Pts',(-20.3279739625217,23.4948873762799,-47.0645599339599));
#18987=CARTESIAN_POINT('Ctrl Pts',(-20.3281302932074,23.486568512563,-47.065069781156));
#18988=CARTESIAN_POINT('Ctrl Pts',(-20.3281937123897,23.4834368233929,-47.0652618653115));
#18989=CARTESIAN_POINT('Ctrl Pts',(-20.3283351824986,23.4769202680563,-47.0656618743923));
#18990=CARTESIAN_POINT('Ctrl Pts',(-20.3284140020381,23.4735354239389,-47.0658698232106));
#18991=CARTESIAN_POINT('Ctrl Pts',(-20.3286071295908,23.4657676902345,-47.0663474408824));
#18992=CARTESIAN_POINT('Ctrl Pts',(-20.3287250477481,23.461384904256,-47.0666172227831));
#18993=CARTESIAN_POINT('Ctrl Pts',(-20.3291258365591,23.4475393347061,-47.0674704279294));
#18994=CARTESIAN_POINT('Ctrl Pts',(-20.3294414580854,23.4380776147196,-47.0680548786724));
#18995=CARTESIAN_POINT('Ctrl Pts',(-20.3324296689895,23.3589606434352,-47.0729537726236));
#18996=CARTESIAN_POINT('Ctrl Pts',(-20.3373196481172,23.2894123079943,-47.0773375420822));
#18997=CARTESIAN_POINT('Ctrl Pts',(-20.3454350314713,23.2106161187651,-47.0823981301487));
#18998=CARTESIAN_POINT('Ctrl Pts',(-20.3464517779048,23.2011553679717,-47.08300726854));
#18999=CARTESIAN_POINT('Ctrl Pts',(-20.3801025034337,22.9005734793209,-47.1024093181714));
#19000=CARTESIAN_POINT('Ctrl Pts',(-20.4522358843225,22.6152834436127,-47.1224670611751));
#19001=CARTESIAN_POINT('Ctrl Pts',(-20.5855505006402,22.2850802587583,-47.1463780076429));
#19002=CARTESIAN_POINT('Ctrl Pts',(-20.6109553438996,22.2271305394117,-47.1505943250702));
#19003=CARTESIAN_POINT('Ctrl Pts',(-20.667485763366,22.1078598540245,-47.1592659405423));
#19004=CARTESIAN_POINT('Ctrl Pts',(-20.6989026482498,22.0467079358772,-47.1637083577696));
#19005=CARTESIAN_POINT('Ctrl Pts',(-20.7376036926109,21.9769611889129,-47.1687317206941));
#19006=CARTESIAN_POINT('Ctrl Pts',(-20.743003083187,21.9673470754087,-47.1694231705848));
#19007=CARTESIAN_POINT('Ctrl Pts',(-20.7500840792734,21.9548889016379,-47.170317690645));
#19008=CARTESIAN_POINT('Ctrl Pts',(-20.7517207784185,21.9520196011798,-47.1705236095619));
#19009=CARTESIAN_POINT('Ctrl Pts',(-20.7543809879693,21.9473725982048,-47.1708569353029));
#19010=CARTESIAN_POINT('Ctrl Pts',(-20.7554017838038,21.9455933568952,-47.1709845178313));
#19011=CARTESIAN_POINT('Ctrl Pts',(-20.7573645294233,21.9421798569341,-47.1712292061707));
#19012=CARTESIAN_POINT('Ctrl Pts',(-20.758306212477,21.9405454554959,-47.1713463284693));
#19013=CARTESIAN_POINT('Ctrl Pts',(-20.7604745034774,21.9367897585847,-47.1716153836962));
#19014=CARTESIAN_POINT('Ctrl Pts',(-20.7617020992184,21.9346690294988,-47.1717672520724));
#19015=CARTESIAN_POINT('Ctrl Pts',(-20.7656040860108,21.9279458618129,-47.172248526888));
#19016=CARTESIAN_POINT('Ctrl Pts',(-20.7682874794295,21.9233486174671,-47.1725773496111));
#19017=CARTESIAN_POINT('Ctrl Pts',(-20.7911857822933,21.8843410872419,-47.1753653008139));
#19018=CARTESIAN_POINT('Ctrl Pts',(-20.8120279862677,21.8503004840158,-47.177784325062));
#19019=CARTESIAN_POINT('Ctrl Pts',(-20.9790454331558,21.588564369038,-47.1963456171584));
#19020=CARTESIAN_POINT('Ctrl Pts',(-21.1527569379827,21.3796803058727,-47.2110006121102));
#19021=CARTESIAN_POINT('Ctrl Pts',(-21.431746132,21.1191233576879,-47.232510879437));
#19022=CARTESIAN_POINT('Ctrl Pts',(-21.5167955263189,21.0475523447392,-47.2388446238688));
#19023=CARTESIAN_POINT('Ctrl Pts',(-21.670306456883,20.9313685222524,-47.2500983564281));
#19024=CARTESIAN_POINT('Ctrl Pts',(-21.7370828018914,20.8847010850375,-47.2549396878769));
#19025=CARTESIAN_POINT('Ctrl Pts',(-21.8143395975489,20.8349563942568,-47.2605134405143));
#19026=CARTESIAN_POINT('Ctrl Pts',(-21.8231557614661,20.8293402635072,-47.2611490808039));
#19027=CARTESIAN_POINT('Ctrl Pts',(-21.8389422485114,20.8193914893992,-47.2622866271828));
#19028=CARTESIAN_POINT('Ctrl Pts',(-21.8459021231342,20.8150423751377,-47.2627879195581));
#19029=CARTESIAN_POINT('Ctrl Pts',(-21.8564154209942,20.8085284906532,-47.2635448435893));
#19030=CARTESIAN_POINT('Ctrl Pts',(-21.8599565853941,20.8063439165117,-47.263799743835));
#19031=CARTESIAN_POINT('Ctrl Pts',(-21.8660949718367,20.8025734862848,-47.2642415110466));
#19032=CARTESIAN_POINT('Ctrl Pts',(-21.8686902337131,20.8009844361986,-47.2644282601176));
#19033=CARTESIAN_POINT('Ctrl Pts',(-21.8740290866806,20.7977259034166,-47.2648123787922));
#19034=CARTESIAN_POINT('Ctrl Pts',(-21.8767729299815,20.7960568415651,-47.2650097636152));
#19035=CARTESIAN_POINT('Ctrl Pts',(-21.8841387732989,20.7915913184023,-47.2655395688877));
#19036=CARTESIAN_POINT('Ctrl Pts',(-21.888765302435,20.7888023814877,-47.2658722646943));
#19037=CARTESIAN_POINT('Ctrl Pts',(-21.9056040913213,20.7787093587756,-47.2670828836337));
#19038=CARTESIAN_POINT('Ctrl Pts',(-21.9178575418911,20.7714746279035,-47.2679633350704));
#19039=CARTESIAN_POINT('Ctrl Pts',(-22.1292828481976,20.6485251040233,-47.2831475946921));
#19040=CARTESIAN_POINT('Ctrl Pts',(-22.340205051915,20.5544351795862,-47.2982583267488));
#19041=CARTESIAN_POINT('Ctrl Pts',(-22.6701077160021,20.4478307199388,-47.3216100270666));
#19042=CARTESIAN_POINT('Ctrl Pts',(-22.7827648297599,20.4180586934479,-47.3295234546108));
#19043=CARTESIAN_POINT('Ctrl Pts',(-22.9885197852767,20.3754533312228,-47.3436829744536));
#19044=CARTESIAN_POINT('Ctrl Pts',(-23.0810454723112,20.3604655964995,-47.3499450596661));
#19045=CARTESIAN_POINT('Ctrl Pts',(-23.2129113175266,20.344968498332,-47.3586153603607));
#19046=CARTESIAN_POINT('Ctrl Pts',(-23.2518061617596,20.3411132559289,-47.3611414874403));
#19047=CARTESIAN_POINT('Ctrl Pts',(-23.3170911307728,20.3358395215527,-47.3653189617976));
#19048=CARTESIAN_POINT('Ctrl Pts',(-23.3434451365479,20.334036424161,-47.3669882602258));
#19049=CARTESIAN_POINT('Ctrl Pts',(-23.3741744678156,20.3323132680365,-47.3689125308422));
#19050=CARTESIAN_POINT('Ctrl Pts',(-23.3785301049849,20.3320778941289,-47.3691847623406));
#19051=CARTESIAN_POINT('Ctrl Pts',(-23.3851669774262,20.3317327573079,-47.3695987695002));
#19052=CARTESIAN_POINT('Ctrl Pts',(-23.3874478516876,20.3316165761085,-47.3697409055185));
#19053=CARTESIAN_POINT('Ctrl Pts',(-23.3914109224923,20.3314189320698,-47.3699876165936));
#19054=CARTESIAN_POINT('Ctrl Pts',(-23.3930930553839,20.3313363634886,-47.3700922541369));
#19055=CARTESIAN_POINT('Ctrl Pts',(-23.3966173999533,20.3311661379833,-47.3703113202413));
#19056=CARTESIAN_POINT('Ctrl Pts',(-23.3984596169259,20.3310787440668,-47.3704257334943));
#19057=CARTESIAN_POINT('Ctrl Pts',(-23.403010497229,20.330866767588,-47.3707081388022));
#19058=CARTESIAN_POINT('Ctrl Pts',(-23.4057192509209,20.3307440217318,-47.3708760269253));
#19059=CARTESIAN_POINT('Ctrl Pts',(-23.4163741443601,20.3302746744788,-47.3715356250808));
#19060=CARTESIAN_POINT('Ctrl Pts',(-23.4243214884951,20.3299540674094,-47.3720258816204));
#19061=CARTESIAN_POINT('Ctrl Pts',(-23.5690192845518,20.3246532347125,-47.380921861269));
#19062=CARTESIAN_POINT('Ctrl Pts',(-23.7059688843849,20.3283577597362,-47.3888533519137));
#19063=CARTESIAN_POINT('Ctrl Pts',(-23.954186105668,20.3509431142435,-47.4029953352529));
#19064=CARTESIAN_POINT('Ctrl Pts',(-24.0654810817681,20.3669705773545,-47.4092500934105));
#19065=CARTESIAN_POINT('Ctrl Pts',(-24.320680828745,20.4174589333123,-47.423793069435));
#19066=CARTESIAN_POINT('Ctrl Pts',(-24.4634959094615,20.4560745035243,-47.4320889013825));
#19067=CARTESIAN_POINT('Ctrl Pts',(-24.6969895379359,20.5367877465825,-47.4464103239032));
#19068=CARTESIAN_POINT('Ctrl Pts',(-24.7892721830987,20.5735424195685,-47.4522774769329));
#19069=CARTESIAN_POINT('Ctrl Pts',(-24.890412640943,20.6193436956108,-47.4590039587461));
#19070=CARTESIAN_POINT('Ctrl Pts',(-24.9010933914153,20.6242510467542,-47.4597180504822));
#19071=CARTESIAN_POINT('Ctrl Pts',(-24.917488408652,20.6318927620447,-47.4608200733898));
#19072=CARTESIAN_POINT('Ctrl Pts',(-24.9232219342466,20.6345857628224,-47.4612065773598));
#19073=CARTESIAN_POINT('Ctrl Pts',(-24.9338710309585,20.6396259525855,-47.4619265374849));
#19074=CARTESIAN_POINT('Ctrl Pts',(-24.9387886707921,20.6419687380518,-47.4622598401406));
#19075=CARTESIAN_POINT('Ctrl Pts',(-24.9468984305534,20.6458575214774,-47.4628108805329));
#19076=CARTESIAN_POINT('Ctrl Pts',(-24.9500939935174,20.6473963479032,-47.4630283682338));
#19077=CARTESIAN_POINT('Ctrl Pts',(-24.9563440862442,20.6504188064498,-47.4634544456392));
#19078=CARTESIAN_POINT('Ctrl Pts',(-24.959398825031,20.6519019977394,-47.463663019745));
#19079=CARTESIAN_POINT('Ctrl Pts',(-24.9664479487446,20.6553383924866,-47.46414508766));
#19080=CARTESIAN_POINT('Ctrl Pts',(-24.9704406402646,20.6572950365662,-47.4644187015173));
#19081=CARTESIAN_POINT('Ctrl Pts',(-24.9811381219992,20.6625648890244,-47.4651533122397));
#19082=CARTESIAN_POINT('Ctrl Pts',(-24.9878354197033,20.6658931690694,-47.4656148367683));
#19083=CARTESIAN_POINT('Ctrl Pts',(-25.0349227904443,20.6894983830256,-47.468871179256));
#19084=CARTESIAN_POINT('Ctrl Pts',(-25.0748922761995,20.7105987868947,-47.4716948896382));
#19085=CARTESIAN_POINT('Ctrl Pts',(-25.1155887923938,20.7331899140132,-47.4746338884125));
#19086=CARTESIAN_POINT('Ctrl Pts',(-25.1167738788161,20.7338487484984,-47.4747195287587));
#19087=CARTESIAN_POINT('Ctrl Pts',(-25.1288947920409,20.740597240982,-47.4755960251268));
#19088=CARTESIAN_POINT('Ctrl Pts',(-25.1397953446281,20.7467497445412,-47.476389088828));
#19089=CARTESIAN_POINT('Ctrl Pts',(-25.1541113297589,20.7549403251158,-47.4774370316322));
#19090=CARTESIAN_POINT('Ctrl Pts',(-25.1575593317277,20.7569215046375,-47.4776899195798));
#19091=CARTESIAN_POINT('Ctrl Pts',(-25.1653284791891,20.7614047088825,-47.4782608447964));
#19092=CARTESIAN_POINT('Ctrl Pts',(-25.1696474873995,20.7639104005177,-47.4785790090972));
#19093=CARTESIAN_POINT('Ctrl Pts',(-25.1924850528609,20.7772307497336,-47.4802654846703));
#19094=CARTESIAN_POINT('Ctrl Pts',(-25.2109008049985,20.7882198138015,-47.4816398100409));
#19095=CARTESIAN_POINT('Ctrl Pts',(-25.3124456267901,20.85019639283,-47.4892982316818));
#19096=CARTESIAN_POINT('Ctrl Pts',(-25.3933303455758,20.9047489883541,-47.4957021716166));
#19097=CARTESIAN_POINT('Ctrl Pts',(-25.5231927479517,21.0011836452817,-47.5064756413385));
#19098=CARTESIAN_POINT('Ctrl Pts',(-25.5736149346995,21.0410197048902,-47.5107910864128));
#19099=CARTESIAN_POINT('Ctrl Pts',(-25.7129364982711,21.1580220425904,-47.5230666806483));
#19100=CARTESIAN_POINT('Ctrl Pts',(-25.7988478514112,21.2385890884365,-47.531066307469));
#19101=CARTESIAN_POINT('Ctrl Pts',(-25.9457457208314,21.3923041016103,-47.5453575933093));
#19102=CARTESIAN_POINT('Ctrl Pts',(-26.0082724415354,21.4638034066355,-47.5516724899737));
#19103=CARTESIAN_POINT('Ctrl Pts',(-26.0985950253867,21.5767938145125,-47.5610426117928));
#19104=CARTESIAN_POINT('Ctrl Pts',(-26.1287344254795,21.6163392492569,-47.5642160608358));
#19105=CARTESIAN_POINT('Ctrl Pts',(-26.1608998024438,21.6606325665487,-47.5676415001442));
#19106=CARTESIAN_POINT('Ctrl Pts',(-26.1638413587519,21.6647032141632,-47.5679551291323));
#19107=CARTESIAN_POINT('Ctrl Pts',(-26.1681854499258,21.6707444449664,-47.5684188246096));
#19108=CARTESIAN_POINT('Ctrl Pts',(-26.1695952832584,21.6727097326198,-47.5685693954869));
#19109=CARTESIAN_POINT('Ctrl Pts',(-26.1719936168834,21.6760609346103,-47.5688256775558));
#19110=CARTESIAN_POINT('Ctrl Pts',(-26.172983231632,21.6774460451591,-47.5689314665877));
#19111=CARTESIAN_POINT('Ctrl Pts',(-26.1750096448848,21.6802870630739,-47.5691481706702));
#19112=CARTESIAN_POINT('Ctrl Pts',(-26.1760463275236,21.6817430457938,-47.5692590776212));
#19113=CARTESIAN_POINT('Ctrl Pts',(-26.1785332334019,21.685241970796,-47.5695252418675));
#19114=CARTESIAN_POINT('Ctrl Pts',(-26.1799822894141,21.6872857470487,-47.5696804179622));
#19115=CARTESIAN_POINT('Ctrl Pts',(-26.1852308605211,21.6947067575552,-47.5702428072437));
#19116=CARTESIAN_POINT('Ctrl Pts',(-26.1890163117902,21.7000939903794,-47.5706490545481));
#19117=CARTESIAN_POINT('Ctrl Pts',(-26.2509271634519,21.7887784153394,-47.5773043215657));
#19118=CARTESIAN_POINT('Ctrl Pts',(-26.3051061569114,21.8747762208373,-47.5832906013368));
#19119=CARTESIAN_POINT('Ctrl Pts',(-26.4037624409338,22.0491368207772,-47.5948283147031));
#19120=CARTESIAN_POINT('Ctrl Pts',(-26.4484145684482,22.1372677985473,-47.6003814547682));
#19121=CARTESIAN_POINT('Ctrl Pts',(-26.5566916300025,22.3777881095969,-47.6151460053493));
#19122=CARTESIAN_POINT('Ctrl Pts',(-26.6127733276649,22.5332408745153,-47.6243002187779));
#19123=CARTESIAN_POINT('Ctrl Pts',(-26.6910432130484,22.81663740077,-47.6411347831165));
#19124=CARTESIAN_POINT('Ctrl Pts',(-26.7178841376198,22.9429130446096,-47.6486821127377));
#19125=CARTESIAN_POINT('Ctrl Pts',(-26.7391319047749,23.0840392384923,-47.6573126872796));
#19126=CARTESIAN_POINT('Ctrl Pts',(-26.7410912866878,23.0976439575544,-47.6581465939898));
#19127=CARTESIAN_POINT('Ctrl Pts',(-26.7443696239255,23.1214867288704,-47.6596115664574));
#19128=CARTESIAN_POINT('Ctrl Pts',(-26.745726541553,23.1317194255068,-47.6602414271434));
#19129=CARTESIAN_POINT('Ctrl Pts',(-26.7476160382063,23.1465134367289,-47.6611537458396));
#19130=CARTESIAN_POINT('Ctrl Pts',(-26.7481880740367,23.1510697211231,-47.6614349548675));
#19131=CARTESIAN_POINT('Ctrl Pts',(-26.7491675531493,23.159008546947,-47.6619253396636));
#19132=CARTESIAN_POINT('Ctrl Pts',(-26.7495793753157,23.1623905489854,-47.6621343766136));
#19133=CARTESIAN_POINT('Ctrl Pts',(-26.7503634161464,23.1689155329448,-47.662537928585));
#19134=CARTESIAN_POINT('Ctrl Pts',(-26.7507363695441,23.1720584241957,-47.6627324201304));
#19135=CARTESIAN_POINT('Ctrl Pts',(-26.7516078060431,23.1794956574521,-47.6631929269654));
#19136=CARTESIAN_POINT('Ctrl Pts',(-26.752102278165,23.1837904557012,-47.6634590687595));
#19137=CARTESIAN_POINT('Ctrl Pts',(-26.7535478709375,23.196572630649,-47.6642517967511));
#19138=CARTESIAN_POINT('Ctrl Pts',(-26.7544738910744,23.2050627568472,-47.6647791748513));
#19139=CARTESIAN_POINT('Ctrl Pts',(-26.7627072088433,23.2834382303695,-47.6696554605864));
#19140=CARTESIAN_POINT('Ctrl Pts',(-26.7677603403508,23.3535365684622,-47.6740750797761));
#19141=CARTESIAN_POINT('Ctrl Pts',(-26.7707203924583,23.4288820121909,-47.6788935395248));
#19142=CARTESIAN_POINT('Ctrl Pts',(-26.7709100919968,23.4340246348451,-47.6792227543725));
#19143=CARTESIAN_POINT('Ctrl Pts',(-26.7723884515744,23.4768887296141,-47.6819695853973));
#19144=CARTESIAN_POINT('Ctrl Pts',(-26.7730266283869,23.5146284689443,-47.6844061844595));
#19145=CARTESIAN_POINT('Ctrl Pts',(-26.7729035704247,23.7019621054397,-47.6965900601896));
#19146=CARTESIAN_POINT('Ctrl Pts',(-26.7623899232043,23.8513515124925,-47.7065999799563));
#19147=CARTESIAN_POINT('Ctrl Pts',(-26.708452900686,24.2345376627611,-47.7327486043081));
#19148=CARTESIAN_POINT('Ctrl Pts',(-26.6494864425825,24.4652642392901,-47.7489886335974));
#19149=CARTESIAN_POINT('Ctrl Pts',(-26.5607912290871,24.7004559809181,-47.764864332236));
#19150=CARTESIAN_POINT('Ctrl Pts',(-26.5557963518902,24.7134453724226,-47.765738655074));
#19151=CARTESIAN_POINT('Ctrl Pts',(-26.54935950927,24.7298663427011,-47.7668404430173));
#19152=CARTESIAN_POINT('Ctrl Pts',(-26.5479956277592,24.7333280729802,-47.7670725138135));
#19153=CARTESIAN_POINT('Ctrl Pts',(-26.5458280437455,24.7388019031685,-47.7674391499264));
#19154=CARTESIAN_POINT('Ctrl Pts',(-26.5450283073043,24.7408155542676,-47.7675739544661));
#19155=CARTESIAN_POINT('Ctrl Pts',(-26.5435363206126,24.7445612022171,-47.7678245767746));
#19156=CARTESIAN_POINT('Ctrl Pts',(-26.5428446018212,24.7462933935928,-47.7679404256059));
#19157=CARTESIAN_POINT('Ctrl Pts',(-26.5412967289456,24.7501598032785,-47.7681988941076));
#19158=CARTESIAN_POINT('Ctrl Pts',(-26.5404397962093,24.7522937013399,-47.7683414654413));
#19159=CARTESIAN_POINT('Ctrl Pts',(-26.5379228525427,24.7585419423017,-47.7687586998311));
#19160=CARTESIAN_POINT('Ctrl Pts',(-26.5362566201195,24.7626537979144,-47.7690329857462));
#19161=CARTESIAN_POINT('Ctrl Pts',(-26.5239379169787,24.7928739166099,-47.7710468205445));
#19162=CARTESIAN_POINT('Ctrl Pts',(-26.5129512615402,24.8188458646461,-47.7727663945632));
#19163=CARTESIAN_POINT('Ctrl Pts',(-26.4757334853176,24.9037051921803,-47.7783585491426));
#19164=CARTESIAN_POINT('Ctrl Pts',(-26.4480750278351,24.9619532350114,-47.782155089418));
#19165=CARTESIAN_POINT('Ctrl Pts',(-26.3490773334306,25.1552494267479,-47.7947387234217));
#19166=CARTESIAN_POINT('Ctrl Pts',(-26.2698921510799,25.2860526028011,-47.8032352822164));
#19167=CARTESIAN_POINT('Ctrl Pts',(-26.0915808545907,25.5382540526202,-47.8204954181967));
#19168=CARTESIAN_POINT('Ctrl Pts',(-25.9922935529425,25.6590272083428,-47.8292411117475));
#19169=CARTESIAN_POINT('Ctrl Pts',(-25.8671920430915,25.7904646014397,-47.8397567218835));
#19170=CARTESIAN_POINT('Ctrl Pts',(-25.8495182670465,25.8086005673556,-47.8412314554028));
#19171=CARTESIAN_POINT('Ctrl Pts',(-25.8169167073545,25.8412752690036,-47.8439342187483));
#19172=CARTESIAN_POINT('Ctrl Pts',(-25.8020580644704,25.8558811842682,-47.8451595914002));
#19173=CARTESIAN_POINT('Ctrl Pts',(-25.7835649888661,25.873710426203,-47.8466774849437));
#19174=CARTESIAN_POINT('Ctrl Pts',(-25.78006331817,25.8770711698944,-47.846964584204));
#19175=CARTESIAN_POINT('Ctrl Pts',(-25.7736611541424,25.8831879505817,-47.8474889320059));
#19176=CARTESIAN_POINT('Ctrl Pts',(-25.770763090615,25.8859465246214,-47.8477260797917));
#19177=CARTESIAN_POINT('Ctrl Pts',(-25.7637781398705,25.892570526475,-47.8482971644642));
#19178=CARTESIAN_POINT('Ctrl Pts',(-25.7596862637958,25.8964306557096,-47.8486313098547));
#19179=CARTESIAN_POINT('Ctrl Pts',(-25.7505759676133,25.9049800134306,-47.8493743900267));
#19180=CARTESIAN_POINT('Ctrl Pts',(-25.7455526309979,25.9096639432213,-47.8497835334456));
#19181=CARTESIAN_POINT('Ctrl Pts',(-25.7362751132598,25.9182593375862,-47.8505381315842));
#19182=CARTESIAN_POINT('Ctrl Pts',(-25.7320253025991,25.9221754932104,-47.8508833955851));
#19183=CARTESIAN_POINT('Ctrl Pts',(-25.7268084285273,25.9269569041691,-47.851306749717));
#19184=CARTESIAN_POINT('Ctrl Pts',(-25.7258513270892,25.9278330513925,-47.8513843998196));
#19185=CARTESIAN_POINT('Ctrl Pts',(-25.7226911365864,25.930722438502,-47.8516407234415));
#19186=CARTESIAN_POINT('Ctrl Pts',(-25.720485784604,25.9327331920815,-47.8518194971427));
#19187=CARTESIAN_POINT('Ctrl Pts',(-25.712621801844,25.9398832845496,-47.8524566185536));
#19188=CARTESIAN_POINT('Ctrl Pts',(-25.7069477140139,25.9450055219908,-47.8529156555452));
#19189=CARTESIAN_POINT('Ctrl Pts',(-25.6793105875979,25.969776827654,-47.855148400613));
#19190=CARTESIAN_POINT('Ctrl Pts',(-25.6570975093795,25.9891437091238,-47.856933463041));
#19191=CARTESIAN_POINT('Ctrl Pts',(-25.6295800765584,26.0124788077354,-47.8591345835247));
#19192=CARTESIAN_POINT('Ctrl Pts',(-25.6245245212276,26.0167393015084,-47.859538561997));
#19193=CARTESIAN_POINT('Ctrl Pts',(-25.6162118135022,26.0237010785946,-47.8602021491472));
#19194=CARTESIAN_POINT('Ctrl Pts',(-25.6129623704095,26.0264115712651,-47.8604613805459));
#19195=CARTESIAN_POINT('Ctrl Pts',(-25.6071260294127,26.0312604401029,-47.8609266959869));
#19196=CARTESIAN_POINT('Ctrl Pts',(-25.6045411070135,26.0334011934501,-47.8611326826912));
#19197=CARTESIAN_POINT('Ctrl Pts',(-25.5990516558421,26.0379329501982,-47.8615699111964));
#19198=CARTESIAN_POINT('Ctrl Pts',(-25.5961462770467,26.0403229118749,-47.8618011949061));
#19199=CARTESIAN_POINT('Ctrl Pts',(-25.5883848308079,26.0466847159949,-47.8624187152953));
#19200=CARTESIAN_POINT('Ctrl Pts',(-25.5835213573027,26.0506474607845,-47.862805319733));
#19201=CARTESIAN_POINT('Ctrl Pts',(-25.5606622593701,26.0691621952075,-47.8646208378062));
#19202=CARTESIAN_POINT('Ctrl Pts',(-25.5425221560978,26.0835339737648,-47.8660569834112));
#19203=CARTESIAN_POINT('Ctrl Pts',(-25.4020079338285,26.1924158405113,-47.8771489000386));
#19204=CARTESIAN_POINT('Ctrl Pts',(-25.2731483245337,26.2781899388207,-47.8871481763896));
#19205=CARTESIAN_POINT('Ctrl Pts',(-24.8854611873628,26.4977951803487,-47.9167179495369));
#19206=CARTESIAN_POINT('Ctrl Pts',(-24.6140398443489,26.6062521831323,-47.9369236556562));
#19207=CARTESIAN_POINT('Ctrl Pts',(-24.3305363976869,26.6771161750845,-47.9558434141988));
#19208=CARTESIAN_POINT('Ctrl Pts',(-24.3293115995256,26.6774215589014,-47.9559251096147));
#19209=CARTESIAN_POINT('Ctrl Pts',(-24.3207618144074,26.6795479762501,-47.9564950942162));
#19210=CARTESIAN_POINT('Ctrl Pts',(-24.313430561039,26.6813440078023,-47.9569823290274));
#19211=CARTESIAN_POINT('Ctrl Pts',(-24.3034231065928,26.6837584261897,-47.9576452993145));
#19212=CARTESIAN_POINT('Ctrl Pts',(-24.3007523849871,26.6843991581375,-47.9578220222424));
#19213=CARTESIAN_POINT('Ctrl Pts',(-24.2620775509646,26.693625355581,-47.9603781405919));
#19214=CARTESIAN_POINT('Ctrl Pts',(-24.2259270052012,26.7015938123652,-47.9627296414857));
#19215=CARTESIAN_POINT('Ctrl Pts',(-24.1846039363556,26.7099585805031,-47.9653685461465));
#19216=CARTESIAN_POINT('Ctrl Pts',(-24.1795600736413,26.7109670138955,-47.9656898199352));
#19217=CARTESIAN_POINT('Ctrl Pts',(-24.172107495715,26.7124384816562,-47.966163273564));
#19218=CARTESIAN_POINT('Ctrl Pts',(-24.169700663438,26.7129108424495,-47.9663159851364));
#19219=CARTESIAN_POINT('Ctrl Pts',(-24.165441559326,26.7137416785302,-47.9665858799373));
#19220=CARTESIAN_POINT('Ctrl Pts',(-24.1635895107506,26.7141012752443,-47.966703127854));
#19221=CARTESIAN_POINT('Ctrl Pts',(-24.1597648750936,26.7148403880855,-47.9669450174277));
#19222=CARTESIAN_POINT('Ctrl Pts',(-24.1577922531819,26.7152196854642,-47.9670696462005));
#19223=CARTESIAN_POINT('Ctrl Pts',(-24.1526872904146,26.7161963234113,-47.9673918407488));
#19224=CARTESIAN_POINT('Ctrl Pts',(-24.149554405679,26.7167908616176,-47.9675892451703));
#19225=CARTESIAN_POINT('Ctrl Pts',(-24.1427227292941,26.7180768302361,-47.9680190151754));
#19226=CARTESIAN_POINT('Ctrl Pts',(-24.1390235927064,26.7187664356449,-47.9682512770475));
#19227=CARTESIAN_POINT('Ctrl Pts',(-24.1282616904498,26.7207532082102,-47.9689257253198));
#19228=CARTESIAN_POINT('Ctrl Pts',(-24.1211957306731,26.7220332607507,-47.9693669573613));
#19229=CARTESIAN_POINT('Ctrl Pts',(-23.9555121915603,26.751476491219,-47.9796769983529));
#19230=CARTESIAN_POINT('Ctrl Pts',(-23.7949834760435,26.7677348606644,-47.9888978287936));
#19231=CARTESIAN_POINT('Ctrl Pts',(-23.3757520520354,26.7786186633544,-48.0125083363321));
#19232=CARTESIAN_POINT('Ctrl Pts',(-23.1177613781264,26.7542726599896,-48.0266500808854));
#19233=CARTESIAN_POINT('Ctrl Pts',(-22.8454455323168,26.6950551324025,-48.0429752627857));
#19234=CARTESIAN_POINT('Ctrl Pts',(-22.8254918737524,26.6905165757998,-48.0441791865166));
#19235=CARTESIAN_POINT('Ctrl Pts',(-22.8013250602391,26.6847771142227,-48.0456473207597));
#19236=CARTESIAN_POINT('Ctrl Pts',(-22.7970691068637,26.683757190104,-48.0459062476904));
#19237=CARTESIAN_POINT('Ctrl Pts',(-22.7889185141786,26.6817863649306,-48.0464028527255));
#19238=CARTESIAN_POINT('Ctrl Pts',(-22.7850235437187,26.6808368590505,-48.0466404894344));
#19239=CARTESIAN_POINT('Ctrl Pts',(-22.7762118795118,26.6786713469832,-48.0471788347376));
#19240=CARTESIAN_POINT('Ctrl Pts',(-22.7712962679749,26.6774510149827,-48.0474796709734));
#19241=CARTESIAN_POINT('Ctrl Pts',(-22.7596723898274,26.6745362054221,-48.0481922989133));
#19242=CARTESIAN_POINT('Ctrl Pts',(-22.7529666812628,26.6728317070337,-48.0486043897545));
#19243=CARTESIAN_POINT('Ctrl Pts',(-22.7441876507059,26.6705700762383,-48.0491452045463));
#19244=CARTESIAN_POINT('Ctrl Pts',(-22.7421092896663,26.6700324392332,-48.0492733342308));
#19245=CARTESIAN_POINT('Ctrl Pts',(-22.7363855522159,26.6685457013298,-48.0496264660401));
#19246=CARTESIAN_POINT('Ctrl Pts',(-22.7327413079909,26.6675922871627,-48.0498515997971));
#19247=CARTESIAN_POINT('Ctrl Pts',(-22.7264096959591,26.6659239324678,-48.0502432770014));
#19248=CARTESIAN_POINT('Ctrl Pts',(-22.723721561379,26.6652118975012,-48.050409730781));
#19249=CARTESIAN_POINT('Ctrl Pts',(-22.7156619097791,26.6630658839282,-48.0509092936543));
#19250=CARTESIAN_POINT('Ctrl Pts',(-22.7102931975177,26.6616214889843,-48.0512427245238));
#19251=CARTESIAN_POINT('Ctrl Pts',(-22.6926947473034,26.6568379442574,-48.0523378954151));
#19252=CARTESIAN_POINT('Ctrl Pts',(-22.6804810822102,26.6534405533648,-48.0531014495013));
#19253=CARTESIAN_POINT('Ctrl Pts',(-22.6469525549751,26.6439006635392,-48.0552073754439));
#19254=CARTESIAN_POINT('Ctrl Pts',(-22.6256808709784,26.6376101102117,-48.0565544327209));
#19255=CARTESIAN_POINT('Ctrl Pts',(-22.5982987011248,26.629204175539,-48.0583032151905));
#19256=CARTESIAN_POINT('Ctrl Pts',(-22.5921269314877,26.6272891993241,-48.0586983531868));
#19257=CARTESIAN_POINT('Ctrl Pts',(-22.5823310537688,26.6242174058018,-48.0593270815939));
#19258=CARTESIAN_POINT('Ctrl Pts',(-22.578703139882,26.6230727043937,-48.0595602730121));
#19259=CARTESIAN_POINT('Ctrl Pts',(-22.5719145793246,26.6209175124845,-48.0599972637917));
#19260=CARTESIAN_POINT('Ctrl Pts',(-22.568753447111,26.619908558048,-48.0602010122901));
#19261=CARTESIAN_POINT('Ctrl Pts',(-22.5616415380342,26.6176265054982,-48.0606599961497));
#19262=CARTESIAN_POINT('Ctrl Pts',(-22.5576916565996,26.6163506548679,-48.0609153220629));
#19263=CARTESIAN_POINT('Ctrl Pts',(-22.5460779384951,26.6125745158803,-48.0616672654709));
#19264=CARTESIAN_POINT('Ctrl Pts',(-22.5384210474532,26.6100531124611,-48.0621645799476));
#19265=CARTESIAN_POINT('Ctrl Pts',(-22.4801258946871,26.5906138577146,-48.0659628676603));
#19266=CARTESIAN_POINT('Ctrl Pts',(-22.4299081919831,26.5724696019742,-48.0693043348848));
#19267=CARTESIAN_POINT('Ctrl Pts',(-22.276123752642,26.5125458903103,-48.0797624180011));
#19268=CARTESIAN_POINT('Ctrl Pts',(-22.1742777374574,26.466632238947,-48.0870135425246));
#19269=CARTESIAN_POINT('Ctrl Pts',(-22.0750360039475,26.4155367686876,-48.0944001480293));
#19270=CARTESIAN_POINT('',(-26.773002855424,23.551903308829,-47.9332000262529));
#19271=CARTESIAN_POINT('Ctrl Pts',(-22.0750360153631,26.415536774565,-48.3398410585546));
#19272=CARTESIAN_POINT('Ctrl Pts',(-22.1133942443118,26.4352858424012,-48.3372333295926));
#19273=CARTESIAN_POINT('Ctrl Pts',(-22.1521475496805,26.4542638705128,-48.3346679043009));
#19274=CARTESIAN_POINT('Ctrl Pts',(-22.2912003786824,26.5189307592828,-48.3256653736361));
#19275=CARTESIAN_POINT('Ctrl Pts',(-22.3934539284286,26.5602497666329,-48.3194121678932));
#19276=CARTESIAN_POINT('Ctrl Pts',(-22.7224336130672,26.6739370652559,-48.2998564456631));
#19277=CARTESIAN_POINT('Ctrl Pts',(-22.9551302316336,26.7264945517448,-48.2867810556429));
#19278=CARTESIAN_POINT('Ctrl Pts',(-23.2852817073651,26.7634776295853,-48.2674063904904));
#19279=CARTESIAN_POINT('Ctrl Pts',(-23.379482822315,26.76985811539,-48.261795893775));
#19280=CARTESIAN_POINT('Ctrl Pts',(-23.4840874515198,26.7723396174469,-48.2554265425794));
#19281=CARTESIAN_POINT('Ctrl Pts',(-23.4943541427971,26.7725340793388,-48.2547999453092));
#19282=CARTESIAN_POINT('Ctrl Pts',(-23.5087452916319,26.7727378645741,-48.253919522527));
#19283=CARTESIAN_POINT('Ctrl Pts',(-23.5128691806755,26.7727883431962,-48.2536669891383));
#19284=CARTESIAN_POINT('Ctrl Pts',(-23.5204200254212,26.772866273498,-48.2532041532776));
#19285=CARTESIAN_POINT('Ctrl Pts',(-23.5238469547929,26.7728961751435,-48.2529939279742));
#19286=CARTESIAN_POINT('Ctrl Pts',(-23.5307768025355,26.7729455870931,-48.2525684723367));
#19287=CARTESIAN_POINT('Ctrl Pts',(-23.5342797170267,26.7729648524544,-48.2523532346309));
#19288=CARTESIAN_POINT('Ctrl Pts',(-23.5428760226446,26.7729981146558,-48.2518245930969));
#19289=CARTESIAN_POINT('Ctrl Pts',(-23.5479694163242,26.7730057478577,-48.2515109898842));
#19290=CARTESIAN_POINT('Ctrl Pts',(-23.5663893694442,26.772989685574,-48.250375481382));
#19291=CARTESIAN_POINT('Ctrl Pts',(-23.5797155911597,26.7728954036369,-48.2495513634195));
#19292=CARTESIAN_POINT('Ctrl Pts',(-23.7695191525022,26.7703751771359,-48.2377754074615));
#19293=CARTESIAN_POINT('Ctrl Pts',(-23.9454755922586,26.7535395313318,-48.2263629673671));
#19294=CARTESIAN_POINT('Ctrl Pts',(-24.1512149335226,26.7166421605112,-48.2124535675206));
#19295=CARTESIAN_POINT('Ctrl Pts',(-24.1831947318097,26.7104049308991,-48.2102758769589));
#19296=CARTESIAN_POINT('Ctrl Pts',(-24.2411755921231,26.698181131087,-48.2063014122114));
#19297=CARTESIAN_POINT('Ctrl Pts',(-24.2672076602134,26.6923544484336,-48.204507284416));
#19298=CARTESIAN_POINT('Ctrl Pts',(-24.3151279530915,26.681002064407,-48.2011882960618));
#19299=CARTESIAN_POINT('Ctrl Pts',(-24.3370363844787,26.675568228242,-48.1996645572802));
#19300=CARTESIAN_POINT('Ctrl Pts',(-24.3777623792751,26.6650117970623,-48.1968213261261));
#19301=CARTESIAN_POINT('Ctrl Pts',(-24.3965941155757,26.6599476530509,-48.1955023086766));
#19302=CARTESIAN_POINT('Ctrl Pts',(-24.4318514204217,26.6501224299345,-48.1930255314741));
#19303=CARTESIAN_POINT('Ctrl Pts',(-24.4482873601915,26.6454009017314,-48.1918679414845));
#19304=CARTESIAN_POINT('Ctrl Pts',(-24.6150317997973,26.5960604809965,-48.180096883176));
#19305=CARTESIAN_POINT('Ctrl Pts',(-24.7619432714318,26.5406561780747,-48.1694888837999));
#19306=CARTESIAN_POINT('Ctrl Pts',(-24.9096095988687,26.472289638636,-48.1589184976846));
#19307=CARTESIAN_POINT('Ctrl Pts',(-24.9149658794914,26.469791873744,-48.1585352252729));
#19308=CARTESIAN_POINT('Ctrl Pts',(-24.9217285067946,26.4666156177921,-48.1580515320269));
#19309=CARTESIAN_POINT('Ctrl Pts',(-24.9231412371491,26.4659508361634,-48.157950498936));
#19310=CARTESIAN_POINT('Ctrl Pts',(-24.9288541317922,26.4632574745711,-48.157541983339));
#19311=CARTESIAN_POINT('Ctrl Pts',(-24.9331503104697,26.4612203953117,-48.157234885785));
#19312=CARTESIAN_POINT('Ctrl Pts',(-24.9398048549327,26.4580470148486,-48.1567593997401));
#19313=CARTESIAN_POINT('Ctrl Pts',(-24.9421663533241,26.4569173435582,-48.156590701407));
#19314=CARTESIAN_POINT('Ctrl Pts',(-24.9800311540979,26.4387472113551,-48.1538863846729));
#19315=CARTESIAN_POINT('Ctrl Pts',(-25.0152226025531,26.4210592938839,-48.1513818747014));
#19316=CARTESIAN_POINT('Ctrl Pts',(-25.054309184869,26.400507598537,-48.1486175224203));
#19317=CARTESIAN_POINT('Ctrl Pts',(-25.0585305551473,26.3982760159177,-48.1483192011688));
#19318=CARTESIAN_POINT('Ctrl Pts',(-25.0648759791946,26.3949035098945,-48.1478711392579));
#19319=CARTESIAN_POINT('Ctrl Pts',(-25.0670037141435,26.3937695838896,-48.1477209578917));
#19320=CARTESIAN_POINT('Ctrl Pts',(-25.0706846385711,26.3918026152214,-48.147461257962));
#19321=CARTESIAN_POINT('Ctrl Pts',(-25.0722384168639,26.3909706863505,-48.1473516683002));
#19322=CARTESIAN_POINT('Ctrl Pts',(-25.0753585539365,26.3892967979527,-48.1471316710419));
#19323=CARTESIAN_POINT('Ctrl Pts',(-25.0769248960658,26.3884548177782,-48.1470212653897));
#19324=CARTESIAN_POINT('Ctrl Pts',(-25.0806810019198,26.386431730913,-48.1467565944215));
#19325=CARTESIAN_POINT('Ctrl Pts',(-25.0828701024732,26.3852493807927,-48.146602408932));
#19326=CARTESIAN_POINT('Ctrl Pts',(-25.0898268162673,26.3814815932993,-48.1461126333047));
#19327=CARTESIAN_POINT('Ctrl Pts',(-25.0945893055481,26.3788866379254,-48.1457776499571));
#19328=CARTESIAN_POINT('Ctrl Pts',(-25.1056920959117,26.3728006199492,-48.1449973781955));
#19329=CARTESIAN_POINT('Ctrl Pts',(-25.1120272619395,26.3693001798807,-48.1445526767075));
#19330=CARTESIAN_POINT('Ctrl Pts',(-25.1336229717801,26.3572725183588,-48.1430383278276));
#19331=CARTESIAN_POINT('Ctrl Pts',(-25.1488262148281,26.348642312683,-48.1419749348479));
#19332=CARTESIAN_POINT('Ctrl Pts',(-25.194326439302,26.3223220335867,-48.1387982552431));
#19333=CARTESIAN_POINT('Ctrl Pts',(-25.224406470546,26.3042600004006,-48.136706017134));
#19334=CARTESIAN_POINT('Ctrl Pts',(-25.3103737040802,26.2507104426311,-48.1307315603854));
#19335=CARTESIAN_POINT('Ctrl Pts',(-25.3654721946375,26.2139863849008,-48.1269085437208));
#19336=CARTESIAN_POINT('Ctrl Pts',(-25.6618849634079,26.0029505404372,-48.1061550237849));
#19337=CARTESIAN_POINT('Ctrl Pts',(-25.8792748305835,25.7975586816019,-48.0900853051901));
#19338=CARTESIAN_POINT('Ctrl Pts',(-26.0788632534354,25.5484290540982,-48.0714083003768));
#19339=CARTESIAN_POINT('Ctrl Pts',(-26.0921626853434,25.5314830426917,-48.070142252939));
#19340=CARTESIAN_POINT('Ctrl Pts',(-26.108322415936,25.5104619003947,-48.0685763492666));
#19341=CARTESIAN_POINT('Ctrl Pts',(-26.1113446651781,25.5065115598479,-48.0682822790734));
#19342=CARTESIAN_POINT('Ctrl Pts',(-26.1167668782265,25.4993901581752,-48.0677524926499));
#19343=CARTESIAN_POINT('Ctrl Pts',(-26.1191701443562,25.4962216160007,-48.0675168951757));
#19344=CARTESIAN_POINT('Ctrl Pts',(-26.1294738546591,25.482584526293,-48.0665034143078));
#19345=CARTESIAN_POINT('Ctrl Pts',(-26.1373161421172,25.4720723563789,-48.0657234521109));
#19346=CARTESIAN_POINT('Ctrl Pts',(-26.1461884690007,25.4600267534124,-48.0648310339839));
#19347=CARTESIAN_POINT('Ctrl Pts',(-26.1472816963462,25.4585398492817,-48.0647208970747));
#19348=CARTESIAN_POINT('Ctrl Pts',(-26.1525565411491,25.4513525777255,-48.0641886351589));
#19349=CARTESIAN_POINT('Ctrl Pts',(-26.1567206480046,25.4456394315469,-48.0637658708803));
#19350=CARTESIAN_POINT('Ctrl Pts',(-26.1642500206985,25.4352374123322,-48.0629967026498));
#19351=CARTESIAN_POINT('Ctrl Pts',(-26.1676215613572,25.4305531019943,-48.0626505324834));
#19352=CARTESIAN_POINT('Ctrl Pts',(-26.1784869921047,25.4153711719485,-48.06152922832));
#19353=CARTESIAN_POINT('Ctrl Pts',(-26.1859303821194,25.4048377097258,-48.0607522343565));
#19354=CARTESIAN_POINT('Ctrl Pts',(-26.2057522503595,25.3764265758463,-48.058658884286));
#19355=CARTESIAN_POINT('Ctrl Pts',(-26.2180131885803,25.3584680711016,-48.0573381933167));
#19356=CARTESIAN_POINT('Ctrl Pts',(-26.2336533160652,25.3350547382627,-48.0556190503393));
#19357=CARTESIAN_POINT('Ctrl Pts',(-26.2371994610022,25.3297116866843,-48.0552269132274));
#19358=CARTESIAN_POINT('Ctrl Pts',(-26.2428178371051,25.3211912737644,-48.05460185606));
#19359=CARTESIAN_POINT('Ctrl Pts',(-26.2449004592589,25.3180207569838,-48.0543693269339));
#19360=CARTESIAN_POINT('Ctrl Pts',(-26.2486291864632,25.3123223632662,-48.0539515047257));
#19361=CARTESIAN_POINT('Ctrl Pts',(-26.2502773517209,25.309795834224,-48.0537662891761));
#19362=CARTESIAN_POINT('Ctrl Pts',(-26.2541181731114,25.3038900036703,-48.0533334262539));
#19363=CARTESIAN_POINT('Ctrl Pts',(-26.2563080418871,25.3005089030515,-48.053085674987));
#19364=CARTESIAN_POINT('Ctrl Pts',(-26.2625471595148,25.2908361681732,-48.0523770781844));
#19365=CARTESIAN_POINT('Ctrl Pts',(-26.2665808251406,25.2845345573154,-48.0519156524887));
#19366=CARTESIAN_POINT('Ctrl Pts',(-26.2921831911561,25.2442287178093,-48.0489655946774));
#19367=CARTESIAN_POINT('Ctrl Pts',(-26.3131341121019,25.209838081078,-48.0464541871503));
#19368=CARTESIAN_POINT('Ctrl Pts',(-26.3734950587642,25.1064443151658,-48.0389164477733));
#19369=CARTESIAN_POINT('Ctrl Pts',(-26.4110010984762,25.0363706689073,-48.03382348974));
#19370=CARTESIAN_POINT('Ctrl Pts',(-26.5847859626775,24.6806745161146,-48.0080431472434));
#19371=CARTESIAN_POINT('Ctrl Pts',(-26.681040065905,24.3775157549382,-47.9860698081352));
#19372=CARTESIAN_POINT('Ctrl Pts',(-26.7335359402297,24.0532161792036,-47.9644604240851));
#19373=CARTESIAN_POINT('Ctrl Pts',(-26.7354127113856,24.0411907425774,-47.9636620766814));
#19374=CARTESIAN_POINT('Ctrl Pts',(-26.7394487850028,24.0143317335835,-47.9618859432923));
#19375=CARTESIAN_POINT('Ctrl Pts',(-26.741572827519,23.9994930379943,-47.9609094352365));
#19376=CARTESIAN_POINT('Ctrl Pts',(-26.74395815269,23.981957634892,-47.9597614617846));
#19377=CARTESIAN_POINT('Ctrl Pts',(-26.7443196289926,23.9792749877021,-47.9595860050774));
#19378=CARTESIAN_POINT('Ctrl Pts',(-26.7455076698001,23.9703733756249,-47.9590043572596));
#19379=CARTESIAN_POINT('Ctrl Pts',(-26.7463194600648,23.9641524129433,-47.9585987681337));
#19380=CARTESIAN_POINT('Ctrl Pts',(-26.7472810592437,23.9566118797392,-47.9581082679169));
#19381=CARTESIAN_POINT('Ctrl Pts',(-26.7474482190151,23.9552945822239,-47.9580226211536));
#19382=CARTESIAN_POINT('Ctrl Pts',(-26.7481713292853,23.9495677945834,-47.9576504636398));
#19383=CARTESIAN_POINT('Ctrl Pts',(-26.7487189750331,23.9451572372253,-47.9573643087123));
#19384=CARTESIAN_POINT('Ctrl Pts',(-26.7537587620555,23.9038701884394,-47.9546900778334));
#19385=CARTESIAN_POINT('Ctrl Pts',(-26.7576223344678,23.8669177490666,-47.9523298281324));
#19386=CARTESIAN_POINT('Ctrl Pts',(-26.761293094546,23.8247749920161,-47.9496820704458));
#19387=CARTESIAN_POINT('Ctrl Pts',(-26.7617276281419,23.8196440372644,-47.949360442931));
#19388=CARTESIAN_POINT('Ctrl Pts',(-26.7623510857833,23.8120663266482,-47.9488865605085));
#19389=CARTESIAN_POINT('Ctrl Pts',(-26.762549513094,23.8096203936125,-47.9487337725244));
#19390=CARTESIAN_POINT('Ctrl Pts',(-26.7628955735838,23.8052933290219,-47.9484637841957));
#19391=CARTESIAN_POINT('Ctrl Pts',(-26.7630443485005,23.8034122931889,-47.9483465190307));
#19392=CARTESIAN_POINT('Ctrl Pts',(-26.7633276815207,23.7997894946098,-47.9481208695808));
#19393=CARTESIAN_POINT('Ctrl Pts',(-26.76346247498,23.7980477590446,-47.9480124720665));
#19394=CARTESIAN_POINT('Ctrl Pts',(-26.7637497412047,23.7942961950074,-47.9477791803535));
#19395=CARTESIAN_POINT('Ctrl Pts',(-26.7639017449384,23.7922863297547,-47.9476543128028));
#19396=CARTESIAN_POINT('Ctrl Pts',(-26.7642646995405,23.7874265478035,-47.9473526658659));
#19397=CARTESIAN_POINT('Ctrl Pts',(-26.7644737459934,23.7845764841183,-47.9471759936231));
#19398=CARTESIAN_POINT('Ctrl Pts',(-26.7650297785464,23.7768549739956,-47.9466979635083));
#19399=CARTESIAN_POINT('Ctrl Pts',(-26.7653694844485,23.7719829864772,-47.9463970099636));
#19400=CARTESIAN_POINT('Ctrl Pts',(-26.7705290319652,23.6954800720143,-47.9416814422417));
#19401=CARTESIAN_POINT('Ctrl Pts',(-26.7729654280244,23.6237028739272,-47.9373972869849));
#19402=CARTESIAN_POINT('Ctrl Pts',(-26.7730021111297,23.5518989666397,-47.9331984791512));
#19403=CARTESIAN_POINT('Ctrl Pts',(-26.7730021088701,23.5519033837932,-47.9331987374489));
#19404=CARTESIAN_POINT('Ctrl Pts',(-26.773147384322,23.2683005089752,-47.9166147515683));
#19405=CARTESIAN_POINT('Ctrl Pts',(-26.7358584101289,22.9858792144759,-47.9013537634378));
#19406=CARTESIAN_POINT('Ctrl Pts',(-26.6262836614549,22.5791349749879,-47.8773094696323));
#19407=CARTESIAN_POINT('Ctrl Pts',(-26.582043218141,22.448764920814,-47.8692848252479));
#19408=CARTESIAN_POINT('Ctrl Pts',(-26.5213570636572,22.3016033990152,-47.859662947226));
#19409=CARTESIAN_POINT('Ctrl Pts',(-26.5128973020304,22.2816616892274,-47.8583469239738));
#19410=CARTESIAN_POINT('Ctrl Pts',(-26.5017872252828,22.2561899090499,-47.8566497696991));
#19411=CARTESIAN_POINT('Ctrl Pts',(-26.4993211388889,22.2505797005474,-47.8562749545605));
#19412=CARTESIAN_POINT('Ctrl Pts',(-26.4953284812921,22.241566502041,-47.8556711422199));
#19413=CARTESIAN_POINT('Ctrl Pts',(-26.4938119701412,22.2381590497909,-47.8554424908258));
#19414=CARTESIAN_POINT('Ctrl Pts',(-26.4909169383517,22.2316844760013,-47.8550073003305));
#19415=CARTESIAN_POINT('Ctrl Pts',(-26.489539524762,22.228616862411,-47.8548007995544));
#19416=CARTESIAN_POINT('Ctrl Pts',(-26.4863948391397,22.2216426198048,-47.8543306095999));
#19417=CARTESIAN_POINT('Ctrl Pts',(-26.4846245693555,22.2177373566026,-47.8540668173341));
#19418=CARTESIAN_POINT('Ctrl Pts',(-26.4792262008718,22.2058913351981,-47.8532650958377));
#19419=CARTESIAN_POINT('Ctrl Pts',(-26.4755736461966,22.1979618247744,-47.8527263225446));
#19420=CARTESIAN_POINT('Ctrl Pts',(-26.4495652081416,22.1420973134583,-47.8489154970363));
#19421=CARTESIAN_POINT('Ctrl Pts',(-26.4260655786542,22.0947066216884,-47.8456038840066));
#19422=CARTESIAN_POINT('Ctrl Pts',(-26.3998480786388,22.0449505585624,-47.8420392979006));
#19423=CARTESIAN_POINT('Ctrl Pts',(-26.3982799565857,22.0419857786257,-47.8418265623427));
#19424=CARTESIAN_POINT('Ctrl Pts',(-26.3947903095413,22.035412902044,-47.8413541857304));
#19425=CARTESIAN_POINT('Ctrl Pts',(-26.3928665442558,22.0318060069521,-47.8410944679094));
#19426=CARTESIAN_POINT('Ctrl Pts',(-26.3885465894806,22.0237434426945,-47.840512796437));
#19427=CARTESIAN_POINT('Ctrl Pts',(-26.3861467639681,22.0192897430682,-47.8401907187037));
#19428=CARTESIAN_POINT('Ctrl Pts',(-26.3743889621559,21.9975916133996,-47.8386178278566));
#19429=CARTESIAN_POINT('Ctrl Pts',(-26.364884285639,21.9804275197131,-47.8373620292444));
#19430=CARTESIAN_POINT('Ctrl Pts',(-26.2277658042201,21.7380599185687,-47.8194639378452));
#19431=CARTESIAN_POINT('Ctrl Pts',(-26.0736448719002,21.5289735842125,-47.8018702336454));
#19432=CARTESIAN_POINT('Ctrl Pts',(-25.8391703467169,21.2800328928449,-47.7787862027967));
#19433=CARTESIAN_POINT('Ctrl Pts',(-25.779788600825,21.2216881169396,-47.7732008949706));
#19434=CARTESIAN_POINT('Ctrl Pts',(-25.6741105274969,21.125608754104,-47.7637780041608));
#19435=CARTESIAN_POINT('Ctrl Pts',(-25.6289016523962,21.0867410047727,-47.7598961886213));
#19436=CARTESIAN_POINT('Ctrl Pts',(-25.5685190694999,21.0376744324307,-47.7549297632581));
#19437=CARTESIAN_POINT('Ctrl Pts',(-25.5543031504199,21.0263211389551,-47.7537757475303));
#19438=CARTESIAN_POINT('Ctrl Pts',(-25.53412788755,21.0104864606184,-47.7521602082924));
#19439=CARTESIAN_POINT('Ctrl Pts',(-25.5282482763929,21.005904686,-47.7516920278819));
#19440=CARTESIAN_POINT('Ctrl Pts',(-25.5179666463049,20.9979497518961,-47.7508779790647));
#19441=CARTESIAN_POINT('Ctrl Pts',(-25.5135717475837,20.9945675013716,-47.7505314859176));
#19442=CARTESIAN_POINT('Ctrl Pts',(-25.5071705319801,20.9896674752845,-47.7500289795794));
#19443=CARTESIAN_POINT('Ctrl Pts',(-25.505171164584,20.9881407016143,-47.749872331625));
#19444=CARTESIAN_POINT('Ctrl Pts',(-25.5017598987094,20.9855420799565,-47.7496055869691));
#19445=CARTESIAN_POINT('Ctrl Pts',(-25.5003489022511,20.984469054788,-47.74949540625));
#19446=CARTESIAN_POINT('Ctrl Pts',(-25.4975402522987,20.9823368066288,-47.7492763909243));
#19447=CARTESIAN_POINT('Ctrl Pts',(-25.4961426210979,20.9812775614284,-47.7491675546778));
#19448=CARTESIAN_POINT('Ctrl Pts',(-25.4928488015731,20.9787854517268,-47.7489114085107));
#19449=CARTESIAN_POINT('Ctrl Pts',(-25.4909518882989,20.9773535405826,-47.748764166452));
#19450=CARTESIAN_POINT('Ctrl Pts',(-25.4853464607215,20.9731319323172,-47.7483298612345));
#19451=CARTESIAN_POINT('Ctrl Pts',(-25.4816334826611,20.9703481302152,-47.7480432125426));
#19452=CARTESIAN_POINT('Ctrl Pts',(-25.4493301613815,20.9462375634959,-47.7455581500931));
#19453=CARTESIAN_POINT('Ctrl Pts',(-25.4203921673918,20.9253777156906,-47.7433918184966));
#19454=CARTESIAN_POINT('Ctrl Pts',(-25.2997221307899,20.8414020829198,-47.7345750696422));
#19455=CARTESIAN_POINT('Ctrl Pts',(-25.2050879245994,20.7825749230887,-47.7281658391023));
#19456=CARTESIAN_POINT('Ctrl Pts',(-25.0461163003156,20.6948297287179,-47.7178829268279));
#19457=CARTESIAN_POINT('Ctrl Pts',(-24.9835492510793,20.6629166089733,-47.7139505090426));
#19458=CARTESIAN_POINT('Ctrl Pts',(-24.7898331283247,20.5719589317981,-47.7019862929217));
#19459=CARTESIAN_POINT('Ctrl Pts',(-24.6557365507812,20.519626234304,-47.6939829554487));
#19460=CARTESIAN_POINT('Ctrl Pts',(-24.4183861315362,20.4448538564775,-47.6797652406158));
#19461=CARTESIAN_POINT('Ctrl Pts',(-24.3166975432183,20.4182059424897,-47.6736601753268));
#19462=CARTESIAN_POINT('Ctrl Pts',(-24.1668448498245,20.3866717629485,-47.6645308130075));
#19463=CARTESIAN_POINT('Ctrl Pts',(-24.1195804874036,20.3778252799413,-47.6616329994601));
#19464=CARTESIAN_POINT('Ctrl Pts',(-24.0643902763561,20.3687683525638,-47.6582223505244));
#19465=CARTESIAN_POINT('Ctrl Pts',(-24.056638220856,20.3675252837769,-47.6577426777728));
#19466=CARTESIAN_POINT('Ctrl Pts',(-24.0448243097055,20.3656751365731,-47.6570107150606));
#19467=CARTESIAN_POINT('Ctrl Pts',(-24.0407656693459,20.3650474691173,-47.6567590795747));
#19468=CARTESIAN_POINT('Ctrl Pts',(-24.0333982579434,20.3639225166175,-47.6563019852268));
#19469=CARTESIAN_POINT('Ctrl Pts',(-24.0300898862017,20.3634226223867,-47.6560966095309));
#19470=CARTESIAN_POINT('Ctrl Pts',(-24.0229757090799,20.3623590011573,-47.6556547283608));
#19471=CARTESIAN_POINT('Ctrl Pts',(-24.0191696638895,20.3617969357347,-47.6554181704878));
#19472=CARTESIAN_POINT('Ctrl Pts',(-24.0089444579914,20.3603056123116,-47.654782223324));
#19473=CARTESIAN_POINT('Ctrl Pts',(-24.0025235081615,20.3593889190355,-47.6543824361515));
#19474=CARTESIAN_POINT('Ctrl Pts',(-23.9732237069118,20.3552961192214,-47.6525560925661));
#19475=CARTESIAN_POINT('Ctrl Pts',(-23.9503143445909,20.3523467179206,-47.6511223738493));
#19476=CARTESIAN_POINT('Ctrl Pts',(-23.9152659260728,20.3482170122614,-47.6489197979172));
#19477=CARTESIAN_POINT('Ctrl Pts',(-23.9031482605978,20.3468588868687,-47.6481566090561));
#19478=CARTESIAN_POINT('Ctrl Pts',(-23.8788217511065,20.3442721212665,-47.6466210754421));
#19479=CARTESIAN_POINT('Ctrl Pts',(-23.8666130175699,20.3430443750156,-47.6458487160998));
#19480=CARTESIAN_POINT('Ctrl Pts',(-23.8510702808225,20.3415709620217,-47.644863214139));
#19481=CARTESIAN_POINT('Ctrl Pts',(-23.8477423783294,20.341260707965,-47.6446520757404));
#19482=CARTESIAN_POINT('Ctrl Pts',(-23.8335008782966,20.3399553439481,-47.6437479690377));
#19483=CARTESIAN_POINT('Ctrl Pts',(-23.8225828253953,20.3390107367021,-47.6430534499218));
#19484=CARTESIAN_POINT('Ctrl Pts',(-23.8076952315126,20.3377991632403,-47.6421044980782));
#19485=CARTESIAN_POINT('Ctrl Pts',(-23.8037296096592,20.3374838255932,-47.6418515391843));
#19486=CARTESIAN_POINT('Ctrl Pts',(-23.7946895221739,20.3367818192163,-47.6412744661729));
#19487=CARTESIAN_POINT('Ctrl Pts',(-23.7896147131363,20.3363998269343,-47.6409502116259));
#19488=CARTESIAN_POINT('Ctrl Pts',(-23.7632589618185,20.3344787412873,-47.6392646270525));
#19489=CARTESIAN_POINT('Ctrl Pts',(-23.7419644096619,20.3331390223145,-47.6378973594693));
#19490=CARTESIAN_POINT('Ctrl Pts',(-23.4642851162601,20.3184358962199,-47.6199980997976));
#19491=CARTESIAN_POINT('Ctrl Pts',(-23.2072392968542,20.3355471056643,-47.6025395323643));
#19492=CARTESIAN_POINT('Ctrl Pts',(-22.8736050059555,20.3982492060126,-47.5796290440575));
#19493=CARTESIAN_POINT('Ctrl Pts',(-22.7928249908994,20.4166792186849,-47.5740721003254));
#19494=CARTESIAN_POINT('Ctrl Pts',(-22.6635282575336,20.4514712437436,-47.5652424360716));
#19495=CARTESIAN_POINT('Ctrl Pts',(-22.6145347271709,20.4659117267404,-47.5619122901724));
#19496=CARTESIAN_POINT('Ctrl Pts',(-22.5578451162316,20.4840958683256,-47.5580930847178));
#19497=CARTESIAN_POINT('Ctrl Pts',(-22.5497979164179,20.4867121404687,-47.5575517513844));
#19498=CARTESIAN_POINT('Ctrl Pts',(-22.5250865709336,20.4948539431376,-47.5558921163806));
#19499=CARTESIAN_POINT('Ctrl Pts',(-22.5084568578154,20.5004840834936,-47.5547790230891));
#19500=CARTESIAN_POINT('Ctrl Pts',(-22.4850155692696,20.5086344599768,-47.5532161728546));
#19501=CARTESIAN_POINT('Ctrl Pts',(-22.4781655754629,20.5110421340786,-47.5527602266676));
#19502=CARTESIAN_POINT('Ctrl Pts',(-22.4677493800631,20.5147428747101,-47.5520681130539));
#19503=CARTESIAN_POINT('Ctrl Pts',(-22.4641772832026,20.5160191019961,-47.5518309780003));
#19504=CARTESIAN_POINT('Ctrl Pts',(-22.4575852424116,20.5183874176202,-47.5513937732603));
#19505=CARTESIAN_POINT('Ctrl Pts',(-22.4545646672882,20.519477716731,-47.5511935986982));
#19506=CARTESIAN_POINT('Ctrl Pts',(-22.4496529605139,20.5212589364434,-47.5508683636008));
#19507=CARTESIAN_POINT('Ctrl Pts',(-22.4477608472288,20.521947114156,-47.5507431390005));
#19508=CARTESIAN_POINT('Ctrl Pts',(-22.4440982350716,20.523283125029,-47.5505008645502));
#19509=CARTESIAN_POINT('Ctrl Pts',(-22.4423276650325,20.5239307367307,-47.5503838022071));
#19510=CARTESIAN_POINT('Ctrl Pts',(-22.4382637215367,20.5254212275451,-47.5501152420184));
#19511=CARTESIAN_POINT('Ctrl Pts',(-22.4359707322665,20.5262651633285,-47.5499638079247));
#19512=CARTESIAN_POINT('Ctrl Pts',(-22.4287207571431,20.5289428859385,-47.5494852974449));
#19513=CARTESIAN_POINT('Ctrl Pts',(-22.4237672888319,20.5307862716709,-47.5491587952589));
#19514=CARTESIAN_POINT('Ctrl Pts',(-22.3823780507819,20.5463049068447,-47.546434134649));
#19515=CARTESIAN_POINT('Ctrl Pts',(-22.3461862368394,20.5606276679563,-47.5440740927625));
#19516=CARTESIAN_POINT('Ctrl Pts',(-22.3075094257139,20.5767502161452,-47.5415672390349));
#19517=CARTESIAN_POINT('Ctrl Pts',(-22.3047596255157,20.5779009594828,-47.5413890932151));
#19518=CARTESIAN_POINT('Ctrl Pts',(-22.3003102247923,20.5797702145015,-47.5411009681085));
#19519=CARTESIAN_POINT('Ctrl Pts',(-22.2986096441706,20.5804863709535,-47.5409908760492));
#19520=CARTESIAN_POINT('Ctrl Pts',(-22.2942984664424,20.5823062751178,-47.5407118547799));
#19521=CARTESIAN_POINT('Ctrl Pts',(-22.2916887035257,20.5834120091039,-47.5405430200048));
#19522=CARTESIAN_POINT('Ctrl Pts',(-22.2879081636193,20.5850196771776,-47.5402985406211));
#19523=CARTESIAN_POINT('Ctrl Pts',(-22.2867362272803,20.5855188617662,-47.5402227675557));
#19524=CARTESIAN_POINT('Ctrl Pts',(-22.2829853165945,20.5871191847731,-47.5399802899592));
#19525=CARTESIAN_POINT('Ctrl Pts',(-22.2804074766501,20.58822299734,-47.5398137097176));
#19526=CARTESIAN_POINT('Ctrl Pts',(-22.2714029370305,20.5920925920377,-47.5392320491054));
#19527=CARTESIAN_POINT('Ctrl Pts',(-22.2649837635269,20.5948759550989,-47.5388177742811));
#19528=CARTESIAN_POINT('Ctrl Pts',(-22.25411481255,20.5996308579175,-47.5381168871319));
#19529=CARTESIAN_POINT('Ctrl Pts',(-22.2496603713128,20.6015916014402,-47.5378298023229));
#19530=CARTESIAN_POINT('Ctrl Pts',(-22.1133485377821,20.661961944064,-47.5290490600604));
#19531=CARTESIAN_POINT('Ctrl Pts',(-21.9855429453391,20.7291522116693,-47.5209385986133));
#19532=CARTESIAN_POINT('Ctrl Pts',(-21.7396013084066,20.8803229213432,-47.5047864451248));
#19533=CARTESIAN_POINT('Ctrl Pts',(-21.6217699271547,20.9641482832484,-47.4967608580446));
#19534=CARTESIAN_POINT('Ctrl Pts',(-21.4339337403402,21.1177724859014,-47.4829393962682));
#19535=CARTESIAN_POINT('Ctrl Pts',(-21.3607929085943,21.1833920442899,-47.4772613696336));
#19536=CARTESIAN_POINT('Ctrl Pts',(-21.2453553155002,21.2968945635193,-47.4676821147604));
#19537=CARTESIAN_POINT('Ctrl Pts',(-21.2012805010894,21.3428778811891,-47.4638606566956));
#19538=CARTESIAN_POINT('Ctrl Pts',(-21.152967734335,21.3963691211557,-47.4594669750718));
#19539=CARTESIAN_POINT('Ctrl Pts',(-21.1473609649096,21.4026258737268,-47.4589538371114));
#19540=CARTESIAN_POINT('Ctrl Pts',(-21.1389740218879,21.4120590584778,-47.4581813274228));
#19541=CARTESIAN_POINT('Ctrl Pts',(-21.1361754887756,21.4152191803518,-47.4579227269247));
#19542=CARTESIAN_POINT('Ctrl Pts',(-21.1313724533557,21.4206643159967,-47.4574774612566));
#19543=CARTESIAN_POINT('Ctrl Pts',(-21.1293649554274,21.4229466898387,-47.4572909216856));
#19544=CARTESIAN_POINT('Ctrl Pts',(-21.1252366930217,21.4276536244933,-47.4569064197081));
#19545=CARTESIAN_POINT('Ctrl Pts',(-21.1231163291163,21.4300785311292,-47.4567084408764));
#19546=CARTESIAN_POINT('Ctrl Pts',(-21.1180194887726,21.435925084362,-47.4562313625064));
#19547=CARTESIAN_POINT('Ctrl Pts',(-21.1150465981124,21.4393498360819,-47.4559521142895));
#19548=CARTESIAN_POINT('Ctrl Pts',(-21.1059418664999,21.4498832624002,-47.4550938762961));
#19549=CARTESIAN_POINT('Ctrl Pts',(-21.0998338913293,21.4570124166249,-47.4545139002819));
#19550=CARTESIAN_POINT('Ctrl Pts',(-21.0774218033451,21.4834040566216,-47.4523700556633));
#19551=CARTESIAN_POINT('Ctrl Pts',(-21.0613132995523,21.5028307700093,-47.4507981972706));
#19552=CARTESIAN_POINT('Ctrl Pts',(-21.0416350287371,21.5271380372149,-47.4488386269224));
#19553=CARTESIAN_POINT('Ctrl Pts',(-21.0378483123344,21.5318424961323,-47.4484596986602));
#19554=CARTESIAN_POINT('Ctrl Pts',(-21.0297848657579,21.5419180360483,-47.4476488423562));
#19555=CARTESIAN_POINT('Ctrl Pts',(-21.0255120372625,21.5472921885936,-47.4472167619492));
#19556=CARTESIAN_POINT('Ctrl Pts',(-21.0203333791398,21.553848549086,-47.4466901351038));
#19557=CARTESIAN_POINT('Ctrl Pts',(-21.0194111286095,21.5550178155127,-47.4465962354542));
#19558=CARTESIAN_POINT('Ctrl Pts',(-21.0145738899807,21.5611594117836,-47.4461031270948));
#19559=CARTESIAN_POINT('Ctrl Pts',(-21.0106727655152,21.5661425992519,-47.4457033762698));
#19560=CARTESIAN_POINT('Ctrl Pts',(-21.000985667636,21.5785920030382,-47.4447055463073));
#19561=CARTESIAN_POINT('Ctrl Pts',(-20.9952178211088,21.5860721914201,-47.4441067698283));
#19562=CARTESIAN_POINT('Ctrl Pts',(-20.9841192101113,21.600597335083,-47.4429455194635));
#19563=CARTESIAN_POINT('Ctrl Pts',(-20.9787843591245,21.6076390743095,-47.4423832083823));
#19564=CARTESIAN_POINT('Ctrl Pts',(-20.9608138784568,21.6315629555823,-47.4404749998625));
#19565=CARTESIAN_POINT('Ctrl Pts',(-20.9483152122752,21.6485468811345,-47.4391240342816));
#19566=CARTESIAN_POINT('Ctrl Pts',(-20.7611197931617,21.9082194234163,-47.4185241752362));
#19567=CARTESIAN_POINT('Ctrl Pts',(-20.6208849357184,22.1739241579009,-47.3979763336342));
#19568=CARTESIAN_POINT('Ctrl Pts',(-20.4903647942636,22.5351394379514,-47.372275639186));
#19569=CARTESIAN_POINT('Ctrl Pts',(-20.4646117882576,22.6163408430149,-47.3666459920126));
#19570=CARTESIAN_POINT('Ctrl Pts',(-20.4347231242829,22.7254047427757,-47.359357760525));
#19571=CARTESIAN_POINT('Ctrl Pts',(-20.4276925770921,22.7524324932346,-47.3575735649393));
#19572=CARTESIAN_POINT('Ctrl Pts',(-20.4185707794457,22.7894691595945,-47.3551616717672));
#19573=CARTESIAN_POINT('Ctrl Pts',(-20.4161747365096,22.7994008040699,-47.3545181316066));
#19574=CARTESIAN_POINT('Ctrl Pts',(-20.4127063995809,22.8140830235846,-47.3535716978841));
#19575=CARTESIAN_POINT('Ctrl Pts',(-20.4115976079334,22.8188247867374,-47.3532667955687));
#19576=CARTESIAN_POINT('Ctrl Pts',(-20.409612478466,22.8274018585581,-47.3527166688546));
#19577=CARTESIAN_POINT('Ctrl Pts',(-20.4087324105224,22.8312362813486,-47.3524712340588));
#19578=CARTESIAN_POINT('Ctrl Pts',(-20.407401470553,22.8370842294088,-47.3520976922816));
#19579=CARTESIAN_POINT('Ctrl Pts',(-20.4069455112797,22.8390965745571,-47.35196929216));
#19580=CARTESIAN_POINT('Ctrl Pts',(-20.4060892632535,22.8428924782776,-47.3517273553989));
#19581=CARTESIAN_POINT('Ctrl Pts',(-20.4056885605524,22.8446759339904,-47.351613795194));
#19582=CARTESIAN_POINT('Ctrl Pts',(-20.404814728027,22.8485807354448,-47.3513654020984));
#19583=CARTESIAN_POINT('Ctrl Pts',(-20.4043422279676,22.8507022137297,-47.3512306062464));
#19584=CARTESIAN_POINT('Ctrl Pts',(-20.4030604171187,22.8564849795576,-47.3508635984211));
#19585=CARTESIAN_POINT('Ctrl Pts',(-20.4022553462217,22.8601472186875,-47.3506316314891));
#19586=CARTESIAN_POINT('Ctrl Pts',(-20.3984307754859,22.87769101493,-47.3495225695694));
#19587=CARTESIAN_POINT('Ctrl Pts',(-20.3954966313154,22.891591311234,-47.3486503263737));
#19588=CARTESIAN_POINT('Ctrl Pts',(-20.3908096691602,22.9145455320387,-47.3472199539967));
#19589=CARTESIAN_POINT('Ctrl Pts',(-20.3890036621952,22.92358820317,-47.3466590200307));
#19590=CARTESIAN_POINT('Ctrl Pts',(-20.3862706125908,22.9375851026141,-47.3457945352758));
#19591=CARTESIAN_POINT('Ctrl Pts',(-20.3853163552575,22.9425338773559,-47.3454896135562));
#19592=CARTESIAN_POINT('Ctrl Pts',(-20.3836140037037,22.9514750322665,-47.3449399787979));
#19593=CARTESIAN_POINT('Ctrl Pts',(-20.3828618429396,22.9554666156502,-47.3446950664567));
#19594=CARTESIAN_POINT('Ctrl Pts',(-20.3707705677244,23.0203062505158,-47.3407240009115));
#19595=CARTESIAN_POINT('Ctrl Pts',(-20.3611784005086,23.0814713064166,-47.3370824303284));
#19596=CARTESIAN_POINT('Ctrl Pts',(-20.315695004104,23.4384058732049,-47.316240379338));
#19597=CARTESIAN_POINT('Ctrl Pts',(-20.3191924537592,23.7377371569682,-47.300249038256));
#19598=CARTESIAN_POINT('Ctrl Pts',(-20.3761110827618,24.1139501367766,-47.278288685536));
#19599=CARTESIAN_POINT('Ctrl Pts',(-20.3915861853837,24.195042587439,-47.2734522083116));
#19600=CARTESIAN_POINT('Ctrl Pts',(-20.4196857768931,24.3167139577483,-47.265986394354));
#19601=CARTESIAN_POINT('Ctrl Pts',(-20.4300283421045,24.3577870945927,-47.2634296329413));
#19602=CARTESIAN_POINT('Ctrl Pts',(-20.4431746155306,24.4059639147094,-47.2603836350048));
#19603=CARTESIAN_POINT('Ctrl Pts',(-20.4451981345848,24.413277640003,-47.2599199368838));
#19604=CARTESIAN_POINT('Ctrl Pts',(-20.4483415004261,24.4244847253398,-47.2592073993224));
#19605=CARTESIAN_POINT('Ctrl Pts',(-20.4494428983012,24.4283832688448,-47.2589591617686));
#19606=CARTESIAN_POINT('Ctrl Pts',(-20.4514665783504,24.4354950710643,-47.2585056398136));
#19607=CARTESIAN_POINT('Ctrl Pts',(-20.4523865162567,24.4387089956891,-47.2583004322183));
#19608=CARTESIAN_POINT('Ctrl Pts',(-20.454247639724,24.4451730424365,-47.2578871909914));
#19609=CARTESIAN_POINT('Ctrl Pts',(-20.4551889464292,24.4484231249994,-47.2576791536209));
#19610=CARTESIAN_POINT('Ctrl Pts',(-20.4578868470618,24.4576836564633,-47.2570856368946));
#19611=CARTESIAN_POINT('Ctrl Pts',(-20.4596558354621,24.4636904518863,-47.2566997522975));
#19612=CARTESIAN_POINT('Ctrl Pts',(-20.4672781945341,24.489297379722,-47.2550508420696));
#19613=CARTESIAN_POINT('Ctrl Pts',(-20.4733004950927,24.5088463578669,-47.2537822882406));
#19614=CARTESIAN_POINT('Ctrl Pts',(-20.5895740044897,24.8738929946832,-47.2299072153831));
#19615=CARTESIAN_POINT('Ctrl Pts',(-20.7571665682539,25.1983319541831,-47.2051008477312));
#19616=CARTESIAN_POINT('Ctrl Pts',(-21.0100123558617,25.5343566747527,-47.1768981366939));
#19617=CARTESIAN_POINT('Ctrl Pts',(-21.046175207795,25.57980587069,-47.1730320685999));
#19618=CARTESIAN_POINT('Ctrl Pts',(-21.127815212177,25.6769040113041,-47.164697268809));
#19619=CARTESIAN_POINT('Ctrl Pts',(-21.1737607447188,25.7281270701512,-47.160250876277));
#19620=CARTESIAN_POINT('Ctrl Pts',(-21.2263687238229,25.7831284974839,-47.1554576277512));
#19621=CARTESIAN_POINT('Ctrl Pts',(-21.2314410200714,25.7883955581977,-47.154998419822));
#19622=CARTESIAN_POINT('Ctrl Pts',(-21.2391853412541,25.7963826571953,-47.1543018317876));
#19623=CARTESIAN_POINT('Ctrl Pts',(-21.2418442977628,25.7991152498885,-47.1540634691045));
#19624=CARTESIAN_POINT('Ctrl Pts',(-21.2467611019674,25.8041503099204,-47.1536241969889));
#19625=CARTESIAN_POINT('Ctrl Pts',(-21.2490175638551,25.8064541150039,-47.1534231811015));
#19626=CARTESIAN_POINT('Ctrl Pts',(-21.2526906202971,25.8101929937142,-47.1530969135354));
#19627=CARTESIAN_POINT('Ctrl Pts',(-21.2541051033683,25.8116301242302,-47.1529714958614));
#19628=CARTESIAN_POINT('Ctrl Pts',(-21.2568439845844,25.8144076388309,-47.1527290884919));
#19629=CARTESIAN_POINT('Ctrl Pts',(-21.2581682054392,25.8157481848528,-47.1526120858858));
#19630=CARTESIAN_POINT('Ctrl Pts',(-21.261207624226,25.8188196812746,-47.1523439895658));
#19631=CARTESIAN_POINT('Ctrl Pts',(-21.2629236140808,25.820549852158,-47.1521929588693));
#19632=CARTESIAN_POINT('Ctrl Pts',(-21.2683433549751,25.8260019999951,-47.1517169825856));
#19633=CARTESIAN_POINT('Ctrl Pts',(-21.2720542649503,25.8297168967579,-47.1513926025711));
#19634=CARTESIAN_POINT('Ctrl Pts',(-21.3027145482172,25.8602604574713,-47.1487248529345));
#19635=CARTESIAN_POINT('Ctrl Pts',(-21.330129180086,25.8866207002085,-47.1464178565613));
#19636=CARTESIAN_POINT('Ctrl Pts',(-21.3607216682144,25.9150116933644,-47.1439192738293));
#19637=CARTESIAN_POINT('Ctrl Pts',(-21.3634422737156,25.9175277988921,-47.143697718868));
#19638=CARTESIAN_POINT('Ctrl Pts',(-21.3699530437738,25.9235283715593,-47.143169030346));
#19639=CARTESIAN_POINT('Ctrl Pts',(-21.3737472412924,25.9270084700771,-47.142862160856));
#19640=CARTESIAN_POINT('Ctrl Pts',(-21.3851203782429,25.9373900204001,-47.1419459221601));
#19641=CARTESIAN_POINT('Ctrl Pts',(-21.3927239866929,25.9442644811945,-47.1413381300067));
#19642=CARTESIAN_POINT('Ctrl Pts',(-21.4605294885784,26.0049823570778,-47.1359589016551));
#19643=CARTESIAN_POINT('Ctrl Pts',(-21.5227070276251,26.0565848910482,-47.1313097251169));
#19644=CARTESIAN_POINT('Ctrl Pts',(-21.672070481874,26.1713445675928,-47.1206116268679));
#19645=CARTESIAN_POINT('Ctrl Pts',(-21.7606101883463,26.2325785548331,-47.114615818604));
#19646=CARTESIAN_POINT('Ctrl Pts',(-21.9246983669837,26.3343139626544,-47.1038264355563));
#19647=CARTESIAN_POINT('Ctrl Pts',(-21.9990874090174,26.3764339774463,-47.0990452192217));
#19648=CARTESIAN_POINT('Ctrl Pts',(-22.075036119826,26.4155368283487,-47.0942077761624));
#19649=CARTESIAN_POINT('Origin',(-23.5502525316942,23.5502525316942,-77.3107734492734));
#19650=CARTESIAN_POINT('',(-22.075035968613,26.4155367504953,-45.5987738960335));
#19651=CARTESIAN_POINT('',(-22.0750360214967,26.415536777723,-45.8455485119974));
#19652=CARTESIAN_POINT('',(-22.0750360153461,26.4155367745563,-77.3107734492734));
#19653=CARTESIAN_POINT('',(-26.7730016394076,23.5478543589546,-46.4374510733466));
#19654=CARTESIAN_POINT('Ctrl Pts',(-22.075035968613,26.4155367504953,-45.5987738960335));
#19655=CARTESIAN_POINT('Ctrl Pts',(-22.0165580353436,26.3854288766699,-45.6025778778048));
#19656=CARTESIAN_POINT('Ctrl Pts',(-21.9589923427003,26.3535259016668,-45.6063198601432));
#19657=CARTESIAN_POINT('Ctrl Pts',(-21.6136990603566,26.1480877521114,-45.6289827267317));
#19658=CARTESIAN_POINT('Ctrl Pts',(-21.3536432859975,25.9322443973274,-45.6472608830081));
#19659=CARTESIAN_POINT('Ctrl Pts',(-21.1180092056232,25.6646636061829,-45.6688201462336));
#19660=CARTESIAN_POINT('Ctrl Pts',(-21.1045458555812,25.6490761576661,-45.6700716168196));
#19661=CARTESIAN_POINT('Ctrl Pts',(-21.087174758204,25.6285703285659,-45.6717126809756));
#19662=CARTESIAN_POINT('Ctrl Pts',(-21.0831304663481,25.6237678310967,-45.6720966467837));
#19663=CARTESIAN_POINT('Ctrl Pts',(-21.07692618545,25.6163565509976,-45.6726886268114));
#19664=CARTESIAN_POINT('Ctrl Pts',(-21.0747562160286,25.6137561116753,-45.6728962324679));
#19665=CARTESIAN_POINT('Ctrl Pts',(-21.0704732909849,25.6086070783613,-45.6733070981949));
#19666=CARTESIAN_POINT('Ctrl Pts',(-21.0683601548949,25.6060586393545,-45.6735103505449));
#19667=CARTESIAN_POINT('Ctrl Pts',(-21.0637344427058,25.6004625104821,-45.6739564575553));
#19668=CARTESIAN_POINT('Ctrl Pts',(-21.0612235379373,25.5974134516035,-45.6741993797395));
#19669=CARTESIAN_POINT('Ctrl Pts',(-21.0541502303927,25.5887918941537,-45.6748858806032));
#19670=CARTESIAN_POINT('Ctrl Pts',(-21.0496009139492,25.5832087329391,-45.6753299885735));
#19671=CARTESIAN_POINT('Ctrl Pts',(-21.0394558104914,25.570672548558,-45.676326171888));
#19672=CARTESIAN_POINT('Ctrl Pts',(-21.0338701320247,25.5637114549905,-45.6768786506533));
#19673=CARTESIAN_POINT('Ctrl Pts',(-20.9214489946373,25.4224092767963,-45.6880799576363));
#19674=CARTESIAN_POINT('Ctrl Pts',(-20.8255040282504,25.2797921036104,-45.6991648826075));
#19675=CARTESIAN_POINT('Ctrl Pts',(-20.5839922915552,24.8504358265447,-45.7319009234585));
#19676=CARTESIAN_POINT('Ctrl Pts',(-20.4693026896633,24.5487101236792,-45.7543193423022));
#19677=CARTESIAN_POINT('Ctrl Pts',(-20.3976736607389,24.2192988513585,-45.7756515485088));
#19678=CARTESIAN_POINT('Ctrl Pts',(-20.3943721622441,24.2035485096867,-45.7766637686151));
#19679=CARTESIAN_POINT('Ctrl Pts',(-20.3904811574243,24.1842676874093,-45.7778928697495));
#19680=CARTESIAN_POINT('Ctrl Pts',(-20.3897794497448,24.1807604649602,-45.7781160418671));
#19681=CARTESIAN_POINT('Ctrl Pts',(-20.3886317780269,24.1749742019226,-45.778483559913));
#19682=CARTESIAN_POINT('Ctrl Pts',(-20.3881824385008,24.1726958472464,-45.7786280987122));
#19683=CARTESIAN_POINT('Ctrl Pts',(-20.3873763461655,24.1685851946369,-45.7788885652633));
#19684=CARTESIAN_POINT('Ctrl Pts',(-20.3870187235814,24.1667530769632,-45.7790045428694));
#19685=CARTESIAN_POINT('Ctrl Pts',(-20.3862527367308,24.1628106758395,-45.7792538647139));
#19686=CARTESIAN_POINT('Ctrl Pts',(-20.3858448928842,24.1607003001344,-45.7793871784667));
#19687=CARTESIAN_POINT('Ctrl Pts',(-20.3847327436159,24.1549144528182,-45.7797522702867));
#19688=CARTESIAN_POINT('Ctrl Pts',(-20.3840327256504,24.1512381452704,-45.7799838019323));
#19689=CARTESIAN_POINT('Ctrl Pts',(-20.3804173632127,24.1320695782407,-45.7811887398416));
#19690=CARTESIAN_POINT('Ctrl Pts',(-20.3776092487336,24.1165569498306,-45.782156082503));
#19691=CARTESIAN_POINT('Ctrl Pts',(-20.3509120974131,23.9626410773502,-45.7916826035666));
#19692=CARTESIAN_POINT('Ctrl Pts',(-20.3359777592654,23.8228176379373,-45.7997681901704));
#19693=CARTESIAN_POINT('Ctrl Pts',(-20.3189810922899,23.408814198073,-45.8231853555543));
#19694=CARTESIAN_POINT('Ctrl Pts',(-20.342670188454,23.1348797720613,-45.8381075215888));
#19695=CARTESIAN_POINT('Ctrl Pts',(-20.4049382015424,22.8477477104668,-45.855324449209));
#19696=CARTESIAN_POINT('Ctrl Pts',(-20.4093454358813,22.828298342796,-45.856497997509));
#19697=CARTESIAN_POINT('Ctrl Pts',(-20.4151240283008,22.8038520737236,-45.8579829026203));
#19698=CARTESIAN_POINT('Ctrl Pts',(-20.4163273642619,22.7988156275238,-45.8582893525236));
#19699=CARTESIAN_POINT('Ctrl Pts',(-20.4185064964472,22.7897913636945,-45.8588394084121));
#19700=CARTESIAN_POINT('Ctrl Pts',(-20.4194777860636,22.7858024618903,-45.8590828811931));
#19701=CARTESIAN_POINT('Ctrl Pts',(-20.4212551693743,22.7785632916962,-45.8595253619068));
#19702=CARTESIAN_POINT('Ctrl Pts',(-20.4220587130763,22.775312398797,-45.8597242937678));
#19703=CARTESIAN_POINT('Ctrl Pts',(-20.435604053182,22.7208764519669,-45.8630592318811));
#19704=CARTESIAN_POINT('Ctrl Pts',(-20.4495949062555,22.6700130072156,-45.8662323980992));
#19705=CARTESIAN_POINT('Ctrl Pts',(-20.4673461278434,22.611166937673,-45.8699781604755));
#19706=CARTESIAN_POINT('Ctrl Pts',(-20.469899126371,22.602826258172,-45.8705108325926));
#19707=CARTESIAN_POINT('Ctrl Pts',(-20.4737570437703,22.59040283204,-45.8713069065935));
#19708=CARTESIAN_POINT('Ctrl Pts',(-20.4750363123559,22.5863121096867,-45.8715694649342));
#19709=CARTESIAN_POINT('Ctrl Pts',(-20.4773336827149,22.5790169190626,-45.8720384729108));
#19710=CARTESIAN_POINT('Ctrl Pts',(-20.4783486478458,22.5758114632265,-45.872244819006));
#19711=CARTESIAN_POINT('Ctrl Pts',(-20.4804774019647,22.5691248261565,-45.8726758211716));
#19712=CARTESIAN_POINT('Ctrl Pts',(-20.4815920999582,22.5656439413388,-45.8729005069672));
#19713=CARTESIAN_POINT('Ctrl Pts',(-20.4845313154655,22.5565190813885,-45.8734903400546));
#19714=CARTESIAN_POINT('Ctrl Pts',(-20.486365491299,22.5508782530394,-45.8738558057817));
#19715=CARTESIAN_POINT('Ctrl Pts',(-20.4944327139779,22.5262992565031,-45.8754519623203));
#19716=CARTESIAN_POINT('Ctrl Pts',(-20.5008257475127,22.5074144199652,-45.8766879354915));
#19717=CARTESIAN_POINT('Ctrl Pts',(-20.5178676367267,22.4585701898914,-45.8799101756262));
#19718=CARTESIAN_POINT('Ctrl Pts',(-20.5287851614256,22.4287074812179,-45.8819052893778));
#19719=CARTESIAN_POINT('Ctrl Pts',(-20.5781164904373,22.2997225022952,-45.8906345613972));
#19720=CARTESIAN_POINT('Ctrl Pts',(-20.6209760372579,22.20238266801,-45.897514785925));
#19721=CARTESIAN_POINT('Ctrl Pts',(-20.7269662233711,21.9907051172541,-45.9131270333222));
#19722=CARTESIAN_POINT('Ctrl Pts',(-20.7923942729529,21.8777253439123,-45.9219125899876));
#19723=CARTESIAN_POINT('Ctrl Pts',(-20.9855454231276,21.5864877227647,-45.9455603035558));
#19724=CARTESIAN_POINT('Ctrl Pts',(-21.124915775929,21.4167441857732,-45.9604612288683));
#19725=CARTESIAN_POINT('Ctrl Pts',(-21.2894446790957,21.253510016613,-45.9750829089385));
#19726=CARTESIAN_POINT('Ctrl Pts',(-21.2984984398579,21.2446329079144,-45.9758789637071));
#19727=CARTESIAN_POINT('Ctrl Pts',(-21.3102144537941,21.2332803308726,-45.9768978714395));
#19728=CARTESIAN_POINT('Ctrl Pts',(-21.3128286656943,21.2307557729151,-45.977124509184));
#19729=CARTESIAN_POINT('Ctrl Pts',(-21.3168255920612,21.2269089652074,-45.9774699265147));
#19730=CARTESIAN_POINT('Ctrl Pts',(-21.3182052115899,21.225583526551,-45.9775889559404));
#19731=CARTESIAN_POINT('Ctrl Pts',(-21.3207963418269,21.2230985891858,-45.977812137595));
#19732=CARTESIAN_POINT('Ctrl Pts',(-21.3220075728037,21.2219388118779,-45.9779163116334));
#19733=CARTESIAN_POINT('Ctrl Pts',(-21.3247925669511,21.2192762892711,-45.9781554891084));
#19734=CARTESIAN_POINT('Ctrl Pts',(-21.3263669443155,21.2177741948747,-45.9782904412377));
#19735=CARTESIAN_POINT('Ctrl Pts',(-21.3307401528241,21.2136102224128,-45.978664595588));
#19736=CARTESIAN_POINT('Ctrl Pts',(-21.3335422616741,21.2109517685088,-45.978903530524));
#19737=CARTESIAN_POINT('Ctrl Pts',(-21.3489824989436,21.1963557557022,-45.9802157540737));
#19738=CARTESIAN_POINT('Ctrl Pts',(-21.3617125979305,21.1845152725435,-45.9812816193898));
#19739=CARTESIAN_POINT('Ctrl Pts',(-21.5174295384143,21.0420129738234,-45.9941354918279));
#19740=CARTESIAN_POINT('Ctrl Pts',(-21.6718424580248,20.9243748027023,-46.0050273612869));
#19741=CARTESIAN_POINT('Ctrl Pts',(-21.994619412911,20.7216039196989,-46.0263509412829));
#19742=CARTESIAN_POINT('Ctrl Pts',(-22.1617149513185,20.635942027308,-46.0367538669091));
#19743=CARTESIAN_POINT('Ctrl Pts',(-22.3734063939086,20.5497787115827,-46.0499778769603));
#19744=CARTESIAN_POINT('Ctrl Pts',(-22.4118022945988,20.5350011590443,-46.0523768650431));
#19745=CARTESIAN_POINT('Ctrl Pts',(-22.4593732506605,20.5177305312903,-46.0553553279665));
#19746=CARTESIAN_POINT('Ctrl Pts',(-22.4682911618978,20.5145373144202,-46.0559139492672));
#19747=CARTESIAN_POINT('Ctrl Pts',(-22.4816988408589,20.509803041301,-46.0567542790278));
#19748=CARTESIAN_POINT('Ctrl Pts',(-22.4861781939927,20.5082324960368,-46.0570351017341));
#19749=CARTESIAN_POINT('Ctrl Pts',(-22.4944535683765,20.505351508906,-46.0575540623688));
#19750=CARTESIAN_POINT('Ctrl Pts',(-22.4982486052393,20.5040382536044,-46.0577921146944));
#19751=CARTESIAN_POINT('Ctrl Pts',(-22.5064763972298,20.5012082726801,-46.0583083595162));
#19752=CARTESIAN_POINT('Ctrl Pts',(-22.5109100205617,20.4996941145305,-46.0585866294469));
#19753=CARTESIAN_POINT('Ctrl Pts',(-22.521954953952,20.4959489546148,-46.0592800776259));
#19754=CARTESIAN_POINT('Ctrl Pts',(-22.5285702163325,20.4937297533191,-46.0596956160141));
#19755=CARTESIAN_POINT('Ctrl Pts',(-22.5368071427109,20.4909962658855,-46.0602132946096));
#19756=CARTESIAN_POINT('Ctrl Pts',(-22.5384221107824,20.4904617454406,-46.0603148060901));
#19757=CARTESIAN_POINT('Ctrl Pts',(-22.5496166216751,20.4867664298182,-46.061018548245));
#19758=CARTESIAN_POINT('Ctrl Pts',(-22.5592104565531,20.4836493746648,-46.0616221346211));
#19759=CARTESIAN_POINT('Ctrl Pts',(-22.5781465875493,20.4775951313769,-46.0628145064408));
#19760=CARTESIAN_POINT('Ctrl Pts',(-22.5874879536924,20.474655381459,-46.0634032034695));
#19761=CARTESIAN_POINT('Ctrl Pts',(-22.608202369643,20.468240124388,-46.064709811335));
#19762=CARTESIAN_POINT('Ctrl Pts',(-22.6195815100508,20.4647849123068,-46.0654283583065));
#19763=CARTESIAN_POINT('Ctrl Pts',(-22.6371832277268,20.4595464788583,-46.0665411515939));
#19764=CARTESIAN_POINT('Ctrl Pts',(-22.6433925699015,20.4577188669407,-46.0669339625419));
#19765=CARTESIAN_POINT('Ctrl Pts',(-22.661352148811,20.4524915179566,-46.0680708664624));
#19766=CARTESIAN_POINT('Ctrl Pts',(-22.6731161948093,20.4491399847251,-46.0688165078664));
#19767=CARTESIAN_POINT('Ctrl Pts',(-22.6892931252701,20.444630649933,-46.0698432260492));
#19768=CARTESIAN_POINT('Ctrl Pts',(-22.6936899179442,20.4434150946271,-46.0701224208528));
#19769=CARTESIAN_POINT('Ctrl Pts',(-22.7012026739291,20.4413552475152,-46.0705997208565));
#19770=CARTESIAN_POINT('Ctrl Pts',(-22.7043173614008,20.4405062925143,-46.070797674122));
#19771=CARTESIAN_POINT('Ctrl Pts',(-22.7103644309178,20.4388678298487,-46.0711821343374));
#19772=CARTESIAN_POINT('Ctrl Pts',(-22.7132966641218,20.4380777839747,-46.0713686235187));
#19773=CARTESIAN_POINT('Ctrl Pts',(-22.7193553506811,20.4364545443433,-46.0717540878499));
#19774=CARTESIAN_POINT('Ctrl Pts',(-22.7224819495484,20.435621912398,-46.0719530810012));
#19775=CARTESIAN_POINT('Ctrl Pts',(-22.7321693670575,20.433057712472,-46.0725698695383));
#19776=CARTESIAN_POINT('Ctrl Pts',(-22.7387343728662,20.4313421639516,-46.0729881843282));
#19777=CARTESIAN_POINT('Ctrl Pts',(-22.7737857426186,20.4223008010219,-46.0752234103511));
#19778=CARTESIAN_POINT('Ctrl Pts',(-22.8023652241135,20.4153446882904,-46.0770522501172));
#19779=CARTESIAN_POINT('Ctrl Pts',(-22.8826486484254,20.3969643749896,-46.0822089927264));
#19780=CARTESIAN_POINT('Ctrl Pts',(-22.9345428623239,20.3864222242885,-46.0855646568667));
#19781=CARTESIAN_POINT('Ctrl Pts',(-23.1145095619368,20.3544578077146,-46.0972839549419));
#19782=CARTESIAN_POINT('Ctrl Pts',(-23.2435896173721,20.3395007323407,-46.105838033096));
#19783=CARTESIAN_POINT('Ctrl Pts',(-23.6628375659541,20.3164341110151,-46.1339607275463));
#19784=CARTESIAN_POINT('Ctrl Pts',(-23.9532932906882,20.3396722613074,-46.1540792125754));
#19785=CARTESIAN_POINT('Ctrl Pts',(-24.2523256931709,20.4048644980893,-46.1734443658615));
#19786=CARTESIAN_POINT('Ctrl Pts',(-24.2679041569044,20.4083822644858,-46.1744488508876));
#19787=CARTESIAN_POINT('Ctrl Pts',(-24.2869294799187,20.4128272563152,-46.1756696941076));
#19788=CARTESIAN_POINT('Ctrl Pts',(-24.2904014250837,20.4136445070041,-46.1758922460162));
#19789=CARTESIAN_POINT('Ctrl Pts',(-24.2961285957211,20.4150026472226,-46.1762589525115));
#19790=CARTESIAN_POINT('Ctrl Pts',(-24.2983845943666,20.4155402071196,-46.1764032985086));
#19791=CARTESIAN_POINT('Ctrl Pts',(-24.3024551908386,20.4165147944557,-46.1766635581792));
#19792=CARTESIAN_POINT('Ctrl Pts',(-24.3042699846525,20.4169509619584,-46.1767795213428));
#19793=CARTESIAN_POINT('Ctrl Pts',(-24.3081760822386,20.4178933435161,-46.177028968745));
#19794=CARTESIAN_POINT('Ctrl Pts',(-24.3102672524509,20.4184000740372,-46.1771624222164));
#19795=CARTESIAN_POINT('Ctrl Pts',(-24.3160040379381,20.4197962910135,-46.177528284821));
#19796=CARTESIAN_POINT('Ctrl Pts',(-24.3196486242385,20.4206900547257,-46.1777604457879));
#19797=CARTESIAN_POINT('Ctrl Pts',(-24.3387231373438,20.4254030417539,-46.1789741118318));
#19798=CARTESIAN_POINT('Ctrl Pts',(-24.354126565583,20.429330105086,-46.179949448137));
#19799=CARTESIAN_POINT('Ctrl Pts',(-24.5460263904108,20.4797694875027,-46.1920482889384));
#19800=CARTESIAN_POINT('Ctrl Pts',(-24.7183199660161,20.5410881113918,-46.2023685455189));
#19801=CARTESIAN_POINT('Ctrl Pts',(-24.9559136318388,20.6491515694645,-46.2169906174701));
#19802=CARTESIAN_POINT('Ctrl Pts',(-25.0261032001551,20.6842213438887,-46.2213609389931));
#19803=CARTESIAN_POINT('Ctrl Pts',(-25.1816447476865,20.76916710313,-46.2312868364782));
#19804=CARTESIAN_POINT('Ctrl Pts',(-25.2661197870087,20.8204769209934,-46.2368512206316));
#19805=CARTESIAN_POINT('Ctrl Pts',(-25.3916137472444,20.9048309859256,-46.2455263522853));
#19806=CARTESIAN_POINT('Ctrl Pts',(-25.4344039128285,20.935135042783,-46.2485614447882));
#19807=CARTESIAN_POINT('Ctrl Pts',(-25.4931223726926,20.9789089921159,-46.2528501432773));
#19808=CARTESIAN_POINT('Ctrl Pts',(-25.5096890776061,20.9915108071235,-46.2540743473389));
#19809=CARTESIAN_POINT('Ctrl Pts',(-25.5358770730943,21.0118347373889,-46.2560331637053));
#19810=CARTESIAN_POINT('Ctrl Pts',(-25.5455782576202,21.0194532588561,-46.256764047246));
#19811=CARTESIAN_POINT('Ctrl Pts',(-25.5973460143364,21.0605901231864,-46.2606930433605));
#19812=CARTESIAN_POINT('Ctrl Pts',(-25.6386102531276,21.095100369918,-46.2639278050148));
#19813=CARTESIAN_POINT('Ctrl Pts',(-25.6855782360978,21.136421820434,-46.2677399912346));
#19814=CARTESIAN_POINT('Ctrl Pts',(-25.69214286011,21.14224497665,-46.2682758550324));
#19815=CARTESIAN_POINT('Ctrl Pts',(-25.7018861595441,21.1509591451082,-46.2690757739128));
#19816=CARTESIAN_POINT('Ctrl Pts',(-25.7050830066274,21.153829854572,-46.2693389733487));
#19817=CARTESIAN_POINT('Ctrl Pts',(-25.7107722153232,21.1589592471565,-46.2698086980577));
#19818=CARTESIAN_POINT('Ctrl Pts',(-25.713266804345,21.1612154595256,-46.2700151185932));
#19819=CARTESIAN_POINT('Ctrl Pts',(-25.7180810199725,21.1655833622212,-46.2704143685858));
#19820=CARTESIAN_POINT('Ctrl Pts',(-25.7204011055336,21.1676945429397,-46.270607176271));
#19821=CARTESIAN_POINT('Ctrl Pts',(-25.7254160516534,21.1722713363335,-46.2710248048688));
#19822=CARTESIAN_POINT('Ctrl Pts',(-25.7281098079192,21.174738147762,-46.2712496767344));
#19823=CARTESIAN_POINT('Ctrl Pts',(-25.7386709937686,21.1844426327633,-46.272133460234));
#19824=CARTESIAN_POINT('Ctrl Pts',(-25.7465065161628,21.1917147909929,-46.2727938455169));
#19825=CARTESIAN_POINT('Ctrl Pts',(-25.8312572755242,21.2711606250431,-46.2799882969201));
#19826=CARTESIAN_POINT('Ctrl Pts',(-25.9046130369542,21.3470219535522,-46.2866829151918));
#19827=CARTESIAN_POINT('Ctrl Pts',(-26.0179198385658,21.4763301188398,-46.29783967667));
#19828=CARTESIAN_POINT('Ctrl Pts',(-26.0601679719696,21.5276651500236,-46.3022087778334));
#19829=CARTESIAN_POINT('Ctrl Pts',(-26.299050875577,21.8369473528616,-46.3281555348715));
#19830=CARTESIAN_POINT('Ctrl Pts',(-26.4574111655566,22.1220626151391,-46.3508198618096));
#19831=CARTESIAN_POINT('Ctrl Pts',(-26.5755924763332,22.4395568428949,-46.3722538042032));
#19832=CARTESIAN_POINT('Ctrl Pts',(-26.580546123074,22.453143848663,-46.3731638405641));
#19833=CARTESIAN_POINT('Ctrl Pts',(-26.5870050880402,22.4712372244287,-46.3743657043706));
#19834=CARTESIAN_POINT('Ctrl Pts',(-26.5885920457054,22.4757139702297,-46.3746622648242));
#19835=CARTESIAN_POINT('Ctrl Pts',(-26.5909649691406,22.4824551817748,-46.375107598245));
#19836=CARTESIAN_POINT('Ctrl Pts',(-26.5917583061088,22.4847170174911,-46.3752568091337));
#19837=CARTESIAN_POINT('Ctrl Pts',(-26.5931673079274,22.488748533657,-46.3755223890342));
#19838=CARTESIAN_POINT('Ctrl Pts',(-26.5937839523025,22.4905178643814,-46.3756388167044));
#19839=CARTESIAN_POINT('Ctrl Pts',(-26.5950886137476,22.4942718462325,-46.3758855673337));
#19840=CARTESIAN_POINT('Ctrl Pts',(-26.5957762318597,22.4962566273221,-46.3760158660535));
#19841=CARTESIAN_POINT('Ctrl Pts',(-26.5976119500857,22.5015721468608,-46.3763643949824));
#19842=CARTESIAN_POINT('Ctrl Pts',(-26.5987565340152,22.5049041101099,-46.3765824149693));
#19843=CARTESIAN_POINT('Ctrl Pts',(-26.6041616364888,22.5207231150396,-46.3776153903402));
#19844=CARTESIAN_POINT('Ctrl Pts',(-26.6083509903354,22.5332346009201,-46.3784261592266));
#19845=CARTESIAN_POINT('Ctrl Pts',(-26.6414664383251,22.6341887311959,-46.3849208107518));
#19846=CARTESIAN_POINT('Ctrl Pts',(-26.6666295296635,22.7238299216021,-46.3903960046259));
#19847=CARTESIAN_POINT('Ctrl Pts',(-26.7442560136724,23.0548436791869,-46.4099802088258));
#19848=CARTESIAN_POINT('Ctrl Pts',(-26.77281788917,23.3009243090713,-46.4233912076773));
#19849=CARTESIAN_POINT('Ctrl Pts',(-26.7730016394076,23.5478543589546,-46.4374510733466));
#19850=CARTESIAN_POINT('Ctrl Pts',(-26.7730016423177,23.5478582728161,-46.4374512961967));
#19851=CARTESIAN_POINT('Ctrl Pts',(-26.7731184949075,23.7051456001714,-46.4464070291098));
#19852=CARTESIAN_POINT('Ctrl Pts',(-26.7617209856594,23.8622143069203,-46.4555805427443));
#19853=CARTESIAN_POINT('Ctrl Pts',(-26.7376925346768,24.0260819106865,-46.4656481510428));
#19854=CARTESIAN_POINT('Ctrl Pts',(-26.7364482240046,24.0343438234673,-46.4661570432107));
#19855=CARTESIAN_POINT('Ctrl Pts',(-26.7344127238532,24.0475111378039,-46.4669701939533));
#19856=CARTESIAN_POINT('Ctrl Pts',(-26.7336422874599,24.0524197479978,-46.4672737947172));
#19857=CARTESIAN_POINT('Ctrl Pts',(-26.7323011605808,24.0608372197463,-46.4677952318725));
#19858=CARTESIAN_POINT('Ctrl Pts',(-26.7317360085714,24.0643469651105,-46.4680128921738));
#19859=CARTESIAN_POINT('Ctrl Pts',(-26.7306619783229,24.0709473804426,-46.4684226817433));
#19860=CARTESIAN_POINT('Ctrl Pts',(-26.7301543987995,24.0740382600113,-46.4686147695162));
#19861=CARTESIAN_POINT('Ctrl Pts',(-26.7290875719744,24.0804759403122,-46.4690152460477));
#19862=CARTESIAN_POINT('Ctrl Pts',(-26.7285275436922,24.0838226061254,-46.4692236594402));
#19863=CARTESIAN_POINT('Ctrl Pts',(-26.7272240568216,24.0915372283624,-46.4697046049134));
#19864=CARTESIAN_POINT('Ctrl Pts',(-26.7264768749336,24.0959045411449,-46.469977255277));
#19865=CARTESIAN_POINT('Ctrl Pts',(-26.7241236099639,24.1094908626452,-46.470826646969));
#19866=CARTESIAN_POINT('Ctrl Pts',(-26.7224863886345,24.1187043644816,-46.4714043798367));
#19867=CARTESIAN_POINT('Ctrl Pts',(-26.7082586366505,24.1967953672538,-46.4763158875254));
#19868=CARTESIAN_POINT('Ctrl Pts',(-26.6934674928553,24.2652481002497,-46.4807196536279));
#19869=CARTESIAN_POINT('Ctrl Pts',(-26.6746212359348,24.3405025200152,-46.4856765265498));
#19870=CARTESIAN_POINT('Ctrl Pts',(-26.6727567724568,24.3478377051879,-46.4861609027556));
#19871=CARTESIAN_POINT('Ctrl Pts',(-26.6576835994587,24.4062757162355,-46.4900295875302));
#19872=CARTESIAN_POINT('Ctrl Pts',(-26.6432477028271,24.4570512501088,-46.4934507474262));
#19873=CARTESIAN_POINT('Ctrl Pts',(-26.6225758173727,24.5235100343554,-46.4980065634005));
#19874=CARTESIAN_POINT('Ctrl Pts',(-26.6174538962157,24.5395332367675,-46.4991110010633));
#19875=CARTESIAN_POINT('Ctrl Pts',(-26.6060956329998,24.5741296430884,-46.5015085427888));
#19876=CARTESIAN_POINT('Ctrl Pts',(-26.5998149102964,24.5926875067223,-46.5028027149303));
#19877=CARTESIAN_POINT('Ctrl Pts',(-26.5055103472674,24.8631844356457,-46.5217826651902));
#19878=CARTESIAN_POINT('Ctrl Pts',(-26.3867048588624,25.1032696751286,-46.540226619876));
#19879=CARTESIAN_POINT('Ctrl Pts',(-26.201012114542,25.3845140138018,-46.5623849775488));
#19880=CARTESIAN_POINT('Ctrl Pts',(-26.1604427523329,25.4417995942538,-46.5669236662633));
#19881=CARTESIAN_POINT('Ctrl Pts',(-26.1112837936525,25.5066167965359,-46.5720475767282));
#19882=CARTESIAN_POINT('Ctrl Pts',(-26.1044894786437,25.5154792079462,-46.5727479009901));
#19883=CARTESIAN_POINT('Ctrl Pts',(-26.0956163030252,25.5269295027079,-46.5736521834068));
#19884=CARTESIAN_POINT('Ctrl Pts',(-26.0935794266073,25.5295495993394,-46.5738590674778));
#19885=CARTESIAN_POINT('Ctrl Pts',(-26.0902748938611,25.5337867976081,-46.574193572185));
#19886=CARTESIAN_POINT('Ctrl Pts',(-26.0890097385519,25.5354058328394,-46.5743213708168));
#19887=CARTESIAN_POINT('Ctrl Pts',(-26.086580858206,25.5385079822049,-46.5745662070783));
#19888=CARTESIAN_POINT('Ctrl Pts',(-26.0854173837576,25.5399912806832,-46.5746832616708));
#19889=CARTESIAN_POINT('Ctrl Pts',(-26.0827431036422,25.5433945322093,-46.5749517982425));
#19890=CARTESIAN_POINT('Ctrl Pts',(-26.0812314122539,25.5453137932795,-46.5751032164912));
#19891=CARTESIAN_POINT('Ctrl Pts',(-26.0764430676977,25.5513789302333,-46.5755816542551));
#19892=CARTESIAN_POINT('Ctrl Pts',(-26.0731583776459,25.5555184942358,-46.5759080997903));
#19893=CARTESIAN_POINT('Ctrl Pts',(-26.0456097165686,25.5900621371338,-46.5786315746146));
#19894=CARTESIAN_POINT('Ctrl Pts',(-26.0208059720214,25.6200343406938,-46.5809905236041));
#19895=CARTESIAN_POINT('Ctrl Pts',(-25.9935136519419,25.6518237600829,-46.5834971307362));
#19896=CARTESIAN_POINT('Ctrl Pts',(-25.9915598427492,25.6540931014208,-46.5836760949816));
#19897=CARTESIAN_POINT('Ctrl Pts',(-25.8141781590945,25.8595413667278,-46.599880802174));
#19898=CARTESIAN_POINT('Ctrl Pts',(-25.6140322967345,26.0400373000633,-46.6144265851439));
#19899=CARTESIAN_POINT('Ctrl Pts',(-25.3443717270565,26.2281032386562,-46.6329509681757));
#19900=CARTESIAN_POINT('Ctrl Pts',(-25.2939944147815,26.2611770880131,-46.6363675788085));
#19901=CARTESIAN_POINT('Ctrl Pts',(-25.1600263545218,26.3438502925547,-46.6453906473557));
#19902=CARTESIAN_POINT('Ctrl Pts',(-25.0750724138897,26.3911119128342,-46.6510525841636));
#19903=CARTESIAN_POINT('Ctrl Pts',(-24.9465053806826,26.4552065017461,-46.6596234300786));
#19904=CARTESIAN_POINT('Ctrl Pts',(-24.9044499331921,26.4750480188053,-46.6624269787629));
#19905=CARTESIAN_POINT('Ctrl Pts',(-24.8548962124833,26.4971292849785,-46.6657354070103));
#19906=CARTESIAN_POINT('Ctrl Pts',(-24.8477995385892,26.5002609208534,-46.666209328047));
#19907=CARTESIAN_POINT('Ctrl Pts',(-24.8376361491402,26.5047020748432,-46.6668882344434));
#19908=CARTESIAN_POINT('Ctrl Pts',(-24.834578560702,26.5060325188655,-46.667092503166));
#19909=CARTESIAN_POINT('Ctrl Pts',(-24.8284004338454,26.5087094019919,-46.6675052974828));
#19910=CARTESIAN_POINT('Ctrl Pts',(-24.8252798197861,26.5100556548196,-46.6677138291186));
#19911=CARTESIAN_POINT('Ctrl Pts',(-24.819236918863,26.5126512706072,-46.6681176928903));
#19912=CARTESIAN_POINT('Ctrl Pts',(-24.8163149006211,26.5139012526221,-46.6683130036056));
#19913=CARTESIAN_POINT('Ctrl Pts',(-24.8093670192176,26.5168612692332,-46.6687774669044));
#19914=CARTESIAN_POINT('Ctrl Pts',(-24.805339521502,26.5185674311037,-46.6690467512245));
#19915=CARTESIAN_POINT('Ctrl Pts',(-24.7910927341977,26.5245685934888,-46.6699994888805));
#19916=CARTESIAN_POINT('Ctrl Pts',(-24.7808548599474,26.5288190238772,-46.6706844565143));
#19917=CARTESIAN_POINT('Ctrl Pts',(-24.6383167925666,26.5871358434497,-46.6802259763764));
#19918=CARTESIAN_POINT('Ctrl Pts',(-24.5026041036304,26.6323882093989,-46.6893810592387));
#19919=CARTESIAN_POINT('Ctrl Pts',(-24.2081147414089,26.7092727874002,-46.7094099572248));
#19920=CARTESIAN_POINT('Ctrl Pts',(-24.049043628112,26.7382599382118,-46.7203276045688));
#19921=CARTESIAN_POINT('Ctrl Pts',(-23.8687860598017,26.7572832955246,-46.732596188559));
#19922=CARTESIAN_POINT('Ctrl Pts',(-23.8490684234534,26.7591805451026,-46.7339365784371));
#19923=CARTESIAN_POINT('Ctrl Pts',(-23.654390093876,26.7761027648933,-46.747149233727));
#19924=CARTESIAN_POINT('Ctrl Pts',(-23.4784713051421,26.7769873987355,-46.7589346424501));
#19925=CARTESIAN_POINT('Ctrl Pts',(-23.2912282831935,26.7625992603705,-46.7707738080367));
#19926=CARTESIAN_POINT('Ctrl Pts',(-23.2791239829174,26.7616002842415,-46.7715359130555));
#19927=CARTESIAN_POINT('Ctrl Pts',(-23.2636173294508,26.7602322089864,-46.7725078353246));
#19928=CARTESIAN_POINT('Ctrl Pts',(-23.2602097293672,26.7599261040177,-46.7727211435077));
#19929=CARTESIAN_POINT('Ctrl Pts',(-23.2547335247202,26.759425383988,-46.7730634965432));
#19930=CARTESIAN_POINT('Ctrl Pts',(-23.2526646214662,26.7592341949524,-46.7731927349279));
#19931=CARTESIAN_POINT('Ctrl Pts',(-23.2487253259274,26.7588663190229,-46.7734386148563));
#19932=CARTESIAN_POINT('Ctrl Pts',(-23.2468549171314,26.7586899986782,-46.7735552760045));
#19933=CARTESIAN_POINT('Ctrl Pts',(-23.242597558466,26.7582849083609,-46.7738206248765));
#19934=CARTESIAN_POINT('Ctrl Pts',(-23.2402107122097,26.7580551101822,-46.7739692534737));
#19935=CARTESIAN_POINT('Ctrl Pts',(-23.2327995505412,26.7573332374187,-46.7744303273297));
#19936=CARTESIAN_POINT('Ctrl Pts',(-23.2277761021706,26.756832017922,-46.7747422563615));
#19937=CARTESIAN_POINT('Ctrl Pts',(-23.1896680133286,26.7529392881662,-46.7771041727925));
#19938=CARTESIAN_POINT('Ctrl Pts',(-23.1566349287742,26.7490474686763,-46.7791264286368));
#19939=CARTESIAN_POINT('Ctrl Pts',(-22.8758242412108,26.7115474000657,-46.7961482088612));
#19940=CARTESIAN_POINT('Ctrl Pts',(-22.6326387363219,26.6497139524358,-46.809812340871));
#19941=CARTESIAN_POINT('Ctrl Pts',(-22.2884334891064,26.5180715099323,-46.8304749790125));
#19942=CARTESIAN_POINT('Ctrl Pts',(-22.1802744908533,26.4697197196176,-46.8371684026907));
#19943=CARTESIAN_POINT('Ctrl Pts',(-22.0750360041347,26.415536768784,-46.8440307128639));
#19944=CARTESIAN_POINT('Ctrl Pts',(-22.075036119826,26.4155368283487,-47.0942077761624));
#19945=CARTESIAN_POINT('Ctrl Pts',(-22.1330124871448,26.4453864627005,-47.0905150554735));
#19946=CARTESIAN_POINT('Ctrl Pts',(-22.1918977163122,26.473477944352,-47.0867898262114));
#19947=CARTESIAN_POINT('Ctrl Pts',(-22.319582456183,26.5296961542186,-47.0787173477208));
#19948=CARTESIAN_POINT('Ctrl Pts',(-22.3885628141297,26.5572624976775,-47.0743591562471));
#19949=CARTESIAN_POINT('Ctrl Pts',(-22.4996906902738,26.5972773982751,-47.0673028948009));
#19950=CARTESIAN_POINT('Ctrl Pts',(-22.5412484516954,26.6112901332707,-47.0646566665043));
#19951=CARTESIAN_POINT('Ctrl Pts',(-22.5903858961391,26.6267492894881,-47.0615148705455));
#19952=CARTESIAN_POINT('Ctrl Pts',(-22.5977022209877,26.6290224423473,-47.0610467417006));
#19953=CARTESIAN_POINT('Ctrl Pts',(-22.6089143713249,26.6324622209073,-47.0603288120002));
#19954=CARTESIAN_POINT('Ctrl Pts',(-22.6128044501931,26.6336476076934,-47.0600796274143));
#19955=CARTESIAN_POINT('Ctrl Pts',(-22.6198970762396,26.6357942133557,-47.0596251176888));
#19956=CARTESIAN_POINT('Ctrl Pts',(-22.6230989000773,26.6367578185858,-47.0594198711317));
#19957=CARTESIAN_POINT('Ctrl Pts',(-22.6295346098767,26.6386837605029,-47.0590071853025));
#19958=CARTESIAN_POINT('Ctrl Pts',(-22.6327685188655,26.6396460049674,-47.058799743306));
#19959=CARTESIAN_POINT('Ctrl Pts',(-22.6419627763121,26.6423660319385,-47.058209768298));
#19960=CARTESIAN_POINT('Ctrl Pts',(-22.6479266819802,26.6441116490745,-47.0578268377941));
#19961=CARTESIAN_POINT('Ctrl Pts',(-22.6731650542139,26.6514196612096,-47.0562052888221));
#19962=CARTESIAN_POINT('Ctrl Pts',(-22.69248585988,26.6568191760392,-47.0549613662014));
#19963=CARTESIAN_POINT('Ctrl Pts',(-23.0854136996775,26.762684301952,-47.0296075216957));
#19964=CARTESIAN_POINT('Ctrl Pts',(-23.4739950965551,26.7952178787711,-47.0029391143135));
#19965=CARTESIAN_POINT('Ctrl Pts',(-23.9173639981117,26.7525642337943,-46.9732697255462));
#19966=CARTESIAN_POINT('Ctrl Pts',(-23.9756989674553,26.7453373769415,-46.9693937319517));
#19967=CARTESIAN_POINT('Ctrl Pts',(-24.0806142091689,26.7294152292454,-46.9625085289852));
#19968=CARTESIAN_POINT('Ctrl Pts',(-24.1272626093662,26.7212805853694,-46.9594781666081));
#19969=CARTESIAN_POINT('Ctrl Pts',(-24.1794910982479,26.7109820387632,-46.9561329232489));
#19970=CARTESIAN_POINT('Ctrl Pts',(-24.1852614114,26.7098278060737,-46.9557639913551));
#19971=CARTESIAN_POINT('Ctrl Pts',(-24.1942237084996,26.7080095386474,-46.9551920331907));
#19972=CARTESIAN_POINT('Ctrl Pts',(-24.1974178644855,26.7073564615284,-46.9549883966249));
#19973=CARTESIAN_POINT('Ctrl Pts',(-24.2027478694714,26.7062582599145,-46.9546489487162));
#19974=CARTESIAN_POINT('Ctrl Pts',(-24.2048842581659,26.7058158134465,-46.9545129854842));
#19975=CARTESIAN_POINT('Ctrl Pts',(-24.2089962855683,26.7049598562067,-46.9542514751177));
#19976=CARTESIAN_POINT('Ctrl Pts',(-24.2109719873206,26.7045466583748,-46.9541259100718));
#19977=CARTESIAN_POINT('Ctrl Pts',(-24.2147334684804,26.7037562939214,-46.953887009438));
#19978=CARTESIAN_POINT('Ctrl Pts',(-24.2165193036891,26.7033794689252,-46.9537736553027));
#19979=CARTESIAN_POINT('Ctrl Pts',(-24.2205830006119,26.7025183910443,-46.9535158711941));
#19980=CARTESIAN_POINT('Ctrl Pts',(-24.2228606539795,26.702033187056,-46.9533714970115));
#19981=CARTESIAN_POINT('Ctrl Pts',(-24.2286554661443,26.7007921620787,-46.9530044569959));
#19982=CARTESIAN_POINT('Ctrl Pts',(-24.2321718995174,26.7000329177162,-46.952781988154));
#19983=CARTESIAN_POINT('Ctrl Pts',(-24.2516620614176,26.6957905660183,-46.951550338644));
#19984=CARTESIAN_POINT('Ctrl Pts',(-24.2676107550675,26.6921917513006,-46.9505477216402));
#19985=CARTESIAN_POINT('Ctrl Pts',(-24.5914431899217,26.6165247593142,-46.9302838092796));
#19986=CARTESIAN_POINT('Ctrl Pts',(-24.8871475521932,26.499641204892,-46.9133817943598));
#19987=CARTESIAN_POINT('Ctrl Pts',(-25.2124729907998,26.3118925201923,-46.8921162567716));
#19988=CARTESIAN_POINT('Ctrl Pts',(-25.2629915425828,26.2808489738545,-46.8887341087877));
#19989=CARTESIAN_POINT('Ctrl Pts',(-25.3816958190136,26.2033148115728,-46.880551710371));
#19990=CARTESIAN_POINT('Ctrl Pts',(-25.4490054378459,26.1555662854329,-46.8757174453742));
#19991=CARTESIAN_POINT('Ctrl Pts',(-25.5481521782361,26.0793484979839,-46.8682414954455));
#19992=CARTESIAN_POINT('Ctrl Pts',(-25.5813802629199,26.0527411489711,-46.8656720388585));
#19993=CARTESIAN_POINT('Ctrl Pts',(-25.6199069149128,26.0206181001692,-46.8626124404476));
#19994=CARTESIAN_POINT('Ctrl Pts',(-25.6257260834494,26.0157311550627,-46.8621481024007));
#19995=CARTESIAN_POINT('Ctrl Pts',(-25.6346226448806,26.0082059941872,-46.8614347858529));
#19996=CARTESIAN_POINT('Ctrl Pts',(-25.6377124626503,26.0055824543198,-46.8611864113062));
#19997=CARTESIAN_POINT('Ctrl Pts',(-25.6433416006531,26.0007844919388,-46.8607327468616));
#19998=CARTESIAN_POINT('Ctrl Pts',(-25.6458825062066,25.9986119310812,-46.8605275340269));
#19999=CARTESIAN_POINT('Ctrl Pts',(-25.6509872677555,25.9942334176294,-46.8601143746657));
#20000=CARTESIAN_POINT('Ctrl Pts',(-25.6535510405158,25.9920273748689,-46.8599064245482));
#20001=CARTESIAN_POINT('Ctrl Pts',(-25.6608461668602,25.9857301426175,-46.8593134269374));
#20002=CARTESIAN_POINT('Ctrl Pts',(-25.6655690698663,25.9816292257842,-46.8589279753431));
#20003=CARTESIAN_POINT('Ctrl Pts',(-25.6856425014342,25.964096621346,-46.8572831001916));
#20004=CARTESIAN_POINT('Ctrl Pts',(-25.7008769990905,25.950533344733,-46.8560181817894));
#20005=CARTESIAN_POINT('Ctrl Pts',(-25.9828337876292,25.6946678455981,-46.8322917193505));
#20006=CARTESIAN_POINT('Ctrl Pts',(-26.2071317354619,25.4095044703714,-46.8076625732223));
#20007=CARTESIAN_POINT('Ctrl Pts',(-26.4447442181116,24.9738261989016,-46.7743616586402));
#20008=CARTESIAN_POINT('Ctrl Pts',(-26.5022890901235,24.8503042221108,-46.7653788345486));
#20009=CARTESIAN_POINT('Ctrl Pts',(-26.5539703217729,24.7180841893289,-46.7564868321669));
#20010=CARTESIAN_POINT('Ctrl Pts',(-26.5560715938307,24.7126651563515,-46.7561236337535));
#20011=CARTESIAN_POINT('Ctrl Pts',(-26.5590801625802,24.7048435610338,-46.7556012260144));
#20012=CARTESIAN_POINT('Ctrl Pts',(-26.5599992499383,24.7024455925758,-46.7554413104187));
#20013=CARTESIAN_POINT('Ctrl Pts',(-26.5615927357418,24.6982731506303,-46.7551634892879));
#20014=CARTESIAN_POINT('Ctrl Pts',(-26.5622684334703,24.6964991777259,-46.7550455049079));
#20015=CARTESIAN_POINT('Ctrl Pts',(-26.5635732720719,24.6930643413765,-46.7548173217338));
#20016=CARTESIAN_POINT('Ctrl Pts',(-26.56420260586,24.6914035590408,-46.7547071112235));
#20017=CARTESIAN_POINT('Ctrl Pts',(-26.5657013281483,24.6874386129672,-46.7544442761747));
#20018=CARTESIAN_POINT('Ctrl Pts',(-26.5665694505736,24.6851339671112,-46.7542917283461));
#20019=CARTESIAN_POINT('Ctrl Pts',(-26.5691850651587,24.6781659686935,-46.7538311840202));
#20020=CARTESIAN_POINT('Ctrl Pts',(-26.5709244011678,24.6734995306799,-46.75352367582));
#20021=CARTESIAN_POINT('Ctrl Pts',(-26.5885369767576,24.6259102465299,-46.7503967922341));
#20022=CARTESIAN_POINT('Ctrl Pts',(-26.6035060472169,24.5826552569206,-46.7476304343677));
#20023=CARTESIAN_POINT('Ctrl Pts',(-26.6194177587917,24.5332985336971,-46.7445434031147));
#20024=CARTESIAN_POINT('Ctrl Pts',(-26.6212695132344,24.527498321365,-46.7441817060314));
#20025=CARTESIAN_POINT('Ctrl Pts',(-26.7222290461342,24.2081439302195,-46.7243245233967));
#20026=CARTESIAN_POINT('Ctrl Pts',(-26.7727927939184,23.8812388493818,-46.7068622091694));
#20027=CARTESIAN_POINT('Ctrl Pts',(-26.773035153289,23.4999560933854,-46.6849291560942));
#20028=CARTESIAN_POINT('Ctrl Pts',(-26.7717931189852,23.4476200877005,-46.6818898520361));
#20029=CARTESIAN_POINT('Ctrl Pts',(-26.7688702821422,23.3868849057655,-46.678317954044));
#20030=CARTESIAN_POINT('Ctrl Pts',(-26.7684301183913,23.3784322088236,-46.6778198368517));
#20031=CARTESIAN_POINT('Ctrl Pts',(-26.7640409680229,23.3000891765746,-46.673193425053));
#20032=CARTESIAN_POINT('Ctrl Pts',(-26.7578493740784,23.2303475714157,-46.6690030614743));
#20033=CARTESIAN_POINT('Ctrl Pts',(-26.7482618182816,23.1515775638346,-46.6641700045108));
#20034=CARTESIAN_POINT('Ctrl Pts',(-26.7470907523437,23.14229356907,-46.6635987952765));
#20035=CARTESIAN_POINT('Ctrl Pts',(-26.745305630228,23.1286213034153,-46.6627552272422));
#20036=CARTESIAN_POINT('Ctrl Pts',(-26.744722923658,23.1242289294534,-46.6624838611846));
#20037=CARTESIAN_POINT('Ctrl Pts',(-26.7436779604442,23.1164748138436,-46.6620041617089));
#20038=CARTESIAN_POINT('Ctrl Pts',(-26.7432194480526,23.1131125673906,-46.6617959472037));
#20039=CARTESIAN_POINT('Ctrl Pts',(-26.7422599654973,23.1061587857662,-46.6613648757264));
#20040=CARTESIAN_POINT('Ctrl Pts',(-26.7417582422151,23.1025673608797,-46.6611419951535));
#20041=CARTESIAN_POINT('Ctrl Pts',(-26.7404571869492,23.0933675205467,-46.6605704303623));
#20042=CARTESIAN_POINT('Ctrl Pts',(-26.739649128997,23.0877603692963,-46.6602214697937));
#20043=CARTESIAN_POINT('Ctrl Pts',(-26.7362837278989,23.064836003685,-46.6587922921019));
#20044=CARTESIAN_POINT('Ctrl Pts',(-26.733600133626,23.0475378863215,-46.6577080743013));
#20045=CARTESIAN_POINT('Ctrl Pts',(-26.7150573729905,22.9341208833049,-46.6505602643618));
#20046=CARTESIAN_POINT('Ctrl Pts',(-26.6949893351046,22.8387505728653,-46.6443631592467));
#20047=CARTESIAN_POINT('Ctrl Pts',(-26.6340935951159,22.6029404839351,-46.6285531923041));
#20048=CARTESIAN_POINT('Ctrl Pts',(-26.5879727769467,22.4641017445517,-46.6187946602675));
#20049=CARTESIAN_POINT('Ctrl Pts',(-26.4395708032775,22.1017329182192,-46.5923575114094));
#20050=CARTESIAN_POINT('Ctrl Pts',(-26.3208909208857,21.8859348797931,-46.575527966804));
#20051=CARTESIAN_POINT('Ctrl Pts',(-26.1706697959829,21.6741579505544,-46.5591256829535));
#20052=CARTESIAN_POINT('Ctrl Pts',(-26.1624126350708,21.6626781283301,-46.5582371568628));
#20053=CARTESIAN_POINT('Ctrl Pts',(-26.1518743416585,21.6482284698605,-46.5571199131279));
#20054=CARTESIAN_POINT('Ctrl Pts',(-26.1496634003198,21.6452079888327,-46.5568864340756));
#20055=CARTESIAN_POINT('Ctrl Pts',(-26.146161266654,21.6404409913575,-46.5565180616147));
#20056=CARTESIAN_POINT('Ctrl Pts',(-26.1448735714259,21.638691928393,-46.5563829252218));
#20057=CARTESIAN_POINT('Ctrl Pts',(-26.1424769080871,21.6354434490548,-46.5561319863809));
#20058=CARTESIAN_POINT('Ctrl Pts',(-26.1413684135299,21.6339437028636,-46.556016152221));
#20059=CARTESIAN_POINT('Ctrl Pts',(-26.1388939971074,21.6306019946083,-46.5557580929059));
#20060=CARTESIAN_POINT('Ctrl Pts',(-26.1375274140051,21.6287605321186,-46.5556159153389));
#20061=CARTESIAN_POINT('Ctrl Pts',(-26.1335294800728,21.6233853381248,-46.5552009759156));
#20062=CARTESIAN_POINT('Ctrl Pts',(-26.1308928334417,21.6198555240237,-46.5549285848699));
#20063=CARTESIAN_POINT('Ctrl Pts',(-26.1117827121665,21.5943809503201,-46.5529633361353));
#20064=CARTESIAN_POINT('Ctrl Pts',(-26.0950361539813,21.5726411074351,-46.5512893765287));
#20065=CARTESIAN_POINT('Ctrl Pts',(-26.0414444605985,21.5048783298875,-46.5460723807065));
#20066=CARTESIAN_POINT('Ctrl Pts',(-26.0036113124238,21.4596486788763,-46.5425911882753));
#20067=CARTESIAN_POINT('Ctrl Pts',(-25.9096322750607,21.3533638718184,-46.5343430910105));
#20068=CARTESIAN_POINT('Ctrl Pts',(-25.8523286069484,21.2933875014658,-46.529631358699));
#20069=CARTESIAN_POINT('Ctrl Pts',(-25.6313768652727,21.0793134772969,-46.5123087205326));
#20070=CARTESIAN_POINT('Ctrl Pts',(-25.4540760963841,20.9402578623714,-46.4999710028688));
#20071=CARTESIAN_POINT('Ctrl Pts',(-25.1647515816971,20.7586268058148,-46.480232414632));
#20072=CARTESIAN_POINT('Ctrl Pts',(-25.0624533198982,20.7019152393474,-46.4733286565222));
#20073=CARTESIAN_POINT('Ctrl Pts',(-24.9477683123053,20.6462587868321,-46.46557181216));
#20074=CARTESIAN_POINT('Ctrl Pts',(-24.9382048182414,20.641675822494,-46.4649248879337));
#20075=CARTESIAN_POINT('Ctrl Pts',(-24.9247395316761,20.6353045958309,-46.4640138443326));
#20076=CARTESIAN_POINT('Ctrl Pts',(-24.920856448475,20.6334767629851,-46.4637510989049));
#20077=CARTESIAN_POINT('Ctrl Pts',(-24.9141106898126,20.6303178656993,-46.4632946118325));
#20078=CARTESIAN_POINT('Ctrl Pts',(-24.9112496810858,20.6289832376397,-46.4631009938652));
#20079=CARTESIAN_POINT('Ctrl Pts',(-24.9053541469863,20.6262435786964,-46.4627019867332));
#20080=CARTESIAN_POINT('Ctrl Pts',(-24.9023193879799,20.624839063314,-46.4624965800683));
#20081=CARTESIAN_POINT('Ctrl Pts',(-24.895211877587,20.6215630619481,-46.4620154715268));
#20082=CARTESIAN_POINT('Ctrl Pts',(-24.8911374046532,20.6196953475649,-46.461739639836));
#20083=CARTESIAN_POINT('Ctrl Pts',(-24.8825295161465,20.6157712521831,-46.4611568383128));
#20084=CARTESIAN_POINT('Ctrl Pts',(-24.8779952095606,20.6137168646149,-46.460849800539));
#20085=CARTESIAN_POINT('Ctrl Pts',(-24.8658174851728,20.6082333957536,-46.4600250762262));
#20086=CARTESIAN_POINT('Ctrl Pts',(-24.8581654648535,20.6048236155251,-46.4595067270423));
#20087=CARTESIAN_POINT('Ctrl Pts',(-24.6668382433594,20.5204597897077,-46.4465427181176));
#20088=CARTESIAN_POINT('Ctrl Pts',(-24.4760485194764,20.4568268983653,-46.4334923567176));
#20089=CARTESIAN_POINT('Ctrl Pts',(-23.994870006502,20.3448660316377,-46.400426477945));
#20090=CARTESIAN_POINT('Ctrl Pts',(-23.7013880696028,20.3177063706888,-46.3800632280934));
#20091=CARTESIAN_POINT('Ctrl Pts',(-23.4048492154817,20.3307825077523,-46.3612846846083));
#20092=CARTESIAN_POINT('Ctrl Pts',(-23.4014181101811,20.3309393014148,-46.3610676700417));
#20093=CARTESIAN_POINT('Ctrl Pts',(-23.3851072172945,20.3317108038475,-46.3600372895401));
#20094=CARTESIAN_POINT('Ctrl Pts',(-23.3722307023733,20.3323973344564,-46.3592276280347));
#20095=CARTESIAN_POINT('Ctrl Pts',(-23.3557498050453,20.3333752695618,-46.3581964475166));
#20096=CARTESIAN_POINT('Ctrl Pts',(-23.3521415529839,20.3335954671754,-46.3579710000214));
#20097=CARTESIAN_POINT('Ctrl Pts',(-23.3463958206743,20.333955811521,-46.3576125095075));
#20098=CARTESIAN_POINT('Ctrl Pts',(-23.3442581100167,20.3340920181118,-46.3574792446728));
#20099=CARTESIAN_POINT('Ctrl Pts',(-23.3402568265992,20.3343509700358,-46.3572300168982));
#20100=CARTESIAN_POINT('Ctrl Pts',(-23.3383932374804,20.3344732031463,-46.3571140259975));
#20101=CARTESIAN_POINT('Ctrl Pts',(-23.3342020895015,20.3347517603026,-46.3568533598662));
#20102=CARTESIAN_POINT('Ctrl Pts',(-23.3318745983783,20.3349089913061,-46.356708736798));
#20103=CARTESIAN_POINT('Ctrl Pts',(-23.3249618985641,20.33538351137,-46.3562795955888));
#20104=CARTESIAN_POINT('Ctrl Pts',(-23.3203771708225,20.3357080839843,-46.3559954881318));
#20105=CARTESIAN_POINT('Ctrl Pts',(-23.2833307072301,20.3384104251202,-46.3537038177598));
#20106=CARTESIAN_POINT('Ctrl Pts',(-23.2509045004983,20.3412701488556,-46.3517229846406));
#20107=CARTESIAN_POINT('Ctrl Pts',(-23.1371835504187,20.3530382792884,-46.3448466603966));
#20108=CARTESIAN_POINT('Ctrl Pts',(-23.0561843632333,20.3645494995546,-46.3400756755157));
#20109=CARTESIAN_POINT('Ctrl Pts',(-22.5970652321221,20.4477332922677,-46.3133200499539));
#20110=CARTESIAN_POINT('Ctrl Pts',(-22.2337909285373,20.5835788628724,-46.2928407818915));
#20111=CARTESIAN_POINT('Ctrl Pts',(-21.8859916640033,20.7904073239977,-46.2683612263381));
#20112=CARTESIAN_POINT('Ctrl Pts',(-21.8690630352994,20.8006868103224,-46.2671575171404));
#20113=CARTESIAN_POINT('Ctrl Pts',(-21.8469755647055,20.81437911306,-46.2655705002012));
#20114=CARTESIAN_POINT('Ctrl Pts',(-21.8417300264633,20.8176518222342,-46.2651923693094));
#20115=CARTESIAN_POINT('Ctrl Pts',(-21.8336418869733,20.822730433082,-46.2646074082557));
#20116=CARTESIAN_POINT('Ctrl Pts',(-21.830792624352,20.8245257422136,-46.2644009711096));
#20117=CARTESIAN_POINT('Ctrl Pts',(-21.8251195999338,20.8281127274198,-46.263989205737));
#20118=CARTESIAN_POINT('Ctrl Pts',(-21.822295802351,20.8299043393402,-46.2637838800683));
#20119=CARTESIAN_POINT('Ctrl Pts',(-21.8161052162796,20.833845602083,-46.2633329402335));
#20120=CARTESIAN_POINT('Ctrl Pts',(-21.8127396292087,20.8359971214083,-46.2630872566405));
#20121=CARTESIAN_POINT('Ctrl Pts',(-21.8031235571604,20.8421696035595,-46.2623837873306));
#20122=CARTESIAN_POINT('Ctrl Pts',(-21.7968830003237,20.8462059188769,-46.2619254283299));
#20123=CARTESIAN_POINT('Ctrl Pts',(-21.7829011138335,20.855317983409,-46.2608943419191));
#20124=CARTESIAN_POINT('Ctrl Pts',(-21.7751676031434,20.8604055569928,-46.2603211724284));
#20125=CARTESIAN_POINT('Ctrl Pts',(-21.6320767873944,20.9554252220369,-46.2496622784904));
#20126=CARTESIAN_POINT('Ctrl Pts',(-21.5037131776303,21.0554201105109,-46.2391872215998));
#20127=CARTESIAN_POINT('Ctrl Pts',(-21.152563576092,21.3743634760058,-46.2077409502529));
#20128=CARTESIAN_POINT('Ctrl Pts',(-20.9533618697632,21.6164609730973,-46.1859974222693));
#20129=CARTESIAN_POINT('Ctrl Pts',(-20.7890506496034,21.8883514133137,-46.165646234025));
#20130=CARTESIAN_POINT('Ctrl Pts',(-20.7860660085806,21.8933204185877,-46.1652756175016));
#20131=CARTESIAN_POINT('Ctrl Pts',(-20.7810807664614,21.9016711007082,-46.1646550171362));
#20132=CARTESIAN_POINT('Ctrl Pts',(-20.7790729256724,21.9050484132058,-46.1644046369155));
#20133=CARTESIAN_POINT('Ctrl Pts',(-20.7654705597469,21.9280239858796,-46.1627055238305));
#20134=CARTESIAN_POINT('Ctrl Pts',(-20.7540774627416,21.9477416452648,-46.1612680897028));
#20135=CARTESIAN_POINT('Ctrl Pts',(-20.740854581943,21.9711964949647,-46.1595841013725));
#20136=CARTESIAN_POINT('Ctrl Pts',(-20.7388222086184,21.9748178786069,-46.1593248206375));
#20137=CARTESIAN_POINT('Ctrl Pts',(-20.735591706771,21.9806003063442,-46.1589119810952));
#20138=CARTESIAN_POINT('Ctrl Pts',(-20.734389062758,21.9827588021015,-46.1587581326101));
#20139=CARTESIAN_POINT('Ctrl Pts',(-20.7322711086601,21.9865703925111,-46.158486917287));
#20140=CARTESIAN_POINT('Ctrl Pts',(-20.7313547692201,21.9882229104134,-46.1583694836743));
#20141=CARTESIAN_POINT('Ctrl Pts',(-20.7294511441487,21.9916630204107,-46.1581253348545));
#20142=CARTESIAN_POINT('Ctrl Pts',(-20.7284641060033,21.9934507416918,-46.1579986358084));
#20143=CARTESIAN_POINT('Ctrl Pts',(-20.7259048522426,21.9980964866438,-46.1576698416296));
#20144=CARTESIAN_POINT('Ctrl Pts',(-20.7243352703738,22.000955970346,-46.1574679167065));
#20145=CARTESIAN_POINT('Ctrl Pts',(-20.7176567159525,22.013166958621,-46.1566075237079));
#20146=CARTESIAN_POINT('Ctrl Pts',(-20.7125897236506,22.0225415283679,-46.1559517258786));
#20147=CARTESIAN_POINT('Ctrl Pts',(-20.6320264091037,22.173377516649,-46.1454730549811));
#20148=CARTESIAN_POINT('Ctrl Pts',(-20.5671326875692,22.3202769682032,-46.1362912286893));
#20149=CARTESIAN_POINT('Ctrl Pts',(-20.4105962454914,22.7609113210053,-46.1099589024377));
#20150=CARTESIAN_POINT('Ctrl Pts',(-20.3496821334957,23.0635901017848,-46.0931842016818));
#20151=CARTESIAN_POINT('Ctrl Pts',(-20.3324041733085,23.3725601936962,-46.0746639114791));
#20152=CARTESIAN_POINT('Ctrl Pts',(-20.332280905291,23.374806710498,-46.074529188141));
#20153=CARTESIAN_POINT('Ctrl Pts',(-20.3316531963427,23.3864697303183,-46.0738294305091));
#20154=CARTESIAN_POINT('Ctrl Pts',(-20.3311877386212,23.3958882135158,-46.073263231291));
#20155=CARTESIAN_POINT('Ctrl Pts',(-20.3294508462794,23.4344679791359,-46.0709392789465));
#20156=CARTESIAN_POINT('Ctrl Pts',(-20.3285343119595,23.4636431461924,-46.0691708247247));
#20157=CARTESIAN_POINT('Ctrl Pts',(-20.3278993798856,23.4992695901027,-46.066996668511));
#20158=CARTESIAN_POINT('Ctrl Pts',(-20.327803871908,23.5057134545317,-46.0666028378809));
#20159=CARTESIAN_POINT('Ctrl Pts',(-20.3276782847574,23.5163370966136,-46.0659525726295));
#20160=CARTESIAN_POINT('Ctrl Pts',(-20.3276370075518,23.5205167442933,-46.0656964898248));
#20161=CARTESIAN_POINT('Ctrl Pts',(-20.3275772848037,23.5280478438802,-46.0652346127475));
#20162=CARTESIAN_POINT('Ctrl Pts',(-20.3275559357436,23.5313992721643,-46.0650289099322));
#20163=CARTESIAN_POINT('Ctrl Pts',(-20.3275219270339,23.5384694318735,-46.0645946156991));
#20164=CARTESIAN_POINT('Ctrl Pts',(-20.3275104760203,23.5421881618024,-46.0643659866316));
#20165=CARTESIAN_POINT('Ctrl Pts',(-20.3274971164855,23.5520956537011,-46.0637563302126));
#20166=CARTESIAN_POINT('Ctrl Pts',(-20.3275065982229,23.5582843928995,-46.0633749457714));
#20167=CARTESIAN_POINT('Ctrl Pts',(-20.3275666074314,23.5718839702037,-46.0625356163095));
#20168=CARTESIAN_POINT('Ctrl Pts',(-20.3276248716612,23.5792947232415,-46.0620774300091));
#20169=CARTESIAN_POINT('Ctrl Pts',(-20.3278735737933,23.6012808888444,-46.0607156373471));
#20170=CARTESIAN_POINT('Ctrl Pts',(-20.3281373368476,23.6158551340316,-46.0598097342772));
#20171=CARTESIAN_POINT('Ctrl Pts',(-20.3294024548483,23.6666930435857,-46.0566383627491));
#20172=CARTESIAN_POINT('Ctrl Pts',(-20.3309172057724,23.7029401094892,-46.0543569176981));
#20173=CARTESIAN_POINT('Ctrl Pts',(-20.3407692351601,23.8707326214571,-46.0436984142799));
#20174=CARTESIAN_POINT('Ctrl Pts',(-20.356558828979,24.0016986909128,-46.0350940231204));
#20175=CARTESIAN_POINT('Ctrl Pts',(-20.4368313216917,24.4396162249895,-46.0054450394432));
#20176=CARTESIAN_POINT('Ctrl Pts',(-20.5380114740334,24.7380074249844,-45.9835919345037));
#20177=CARTESIAN_POINT('Ctrl Pts',(-20.687931905263,25.0312969865993,-45.9627509634836));
#20178=CARTESIAN_POINT('Ctrl Pts',(-20.6952982755937,25.0454475913818,-45.9617475911628));
#20179=CARTESIAN_POINT('Ctrl Pts',(-20.7044394368102,25.0626936395594,-45.9605279244867));
#20180=CARTESIAN_POINT('Ctrl Pts',(-20.7061145143444,25.0658412669197,-45.9603054504141));
#20181=CARTESIAN_POINT('Ctrl Pts',(-20.7088875809531,25.0710313309255,-45.9599388414944));
#20182=CARTESIAN_POINT('Ctrl Pts',(-20.7099825507154,25.0730753627264,-45.9597945154271));
#20183=CARTESIAN_POINT('Ctrl Pts',(-20.7119628986108,25.0767626054331,-45.9595342710988));
#20184=CARTESIAN_POINT('Ctrl Pts',(-20.7128474959311,25.0784062247432,-45.9594183033958));
#20185=CARTESIAN_POINT('Ctrl Pts',(-20.7147551199263,25.0819433040308,-45.9591688231514));
#20186=CARTESIAN_POINT('Ctrl Pts',(-20.7157786126209,25.0838365027771,-45.9590353414224));
#20187=CARTESIAN_POINT('Ctrl Pts',(-20.7185927253908,25.089029448095,-45.9586693439844));
#20188=CARTESIAN_POINT('Ctrl Pts',(-20.7203872233828,25.0923271064922,-45.9584370767283));
#20189=CARTESIAN_POINT('Ctrl Pts',(-20.7298195061279,25.1095884254356,-45.9572220442659));
#20190=CARTESIAN_POINT('Ctrl Pts',(-20.7375550676699,25.1234988193722,-45.9562454642447));
#20191=CARTESIAN_POINT('Ctrl Pts',(-20.8352549962929,25.296162590281,-45.9441486338051));
#20192=CARTESIAN_POINT('Ctrl Pts',(-20.9384566120151,25.4470803951999,-45.9338310820955));
#20193=CARTESIAN_POINT('Ctrl Pts',(-21.194929451784,25.7612022840765,-45.9111133885398));
#20194=CARTESIAN_POINT('Ctrl Pts',(-21.3534990623299,25.9188201340518,-45.8987894029577));
#20195=CARTESIAN_POINT('Ctrl Pts',(-21.5984024774316,26.1163386873029,-45.8804187559971));
#20196=CARTESIAN_POINT('Ctrl Pts',(-21.6721554302956,26.1707993491951,-45.8749664249813));
#20197=CARTESIAN_POINT('Ctrl Pts',(-21.7557289257133,26.2271699278189,-45.8688296711048));
#20198=CARTESIAN_POINT('Ctrl Pts',(-21.7633560397364,26.2322671928011,-45.8682700022821));
#20199=CARTESIAN_POINT('Ctrl Pts',(-21.7747420577831,26.2398064372527,-45.8674350409187));
#20200=CARTESIAN_POINT('Ctrl Pts',(-21.7784845075419,26.2422732823821,-45.8671606840082));
#20201=CARTESIAN_POINT('Ctrl Pts',(-21.7849133788009,26.2464916758612,-45.8666895275101));
#20202=CARTESIAN_POINT('Ctrl Pts',(-21.7875972983359,26.2482470415996,-45.8664928713735));
#20203=CARTESIAN_POINT('Ctrl Pts',(-21.7929887513667,26.2517617385734,-45.8660979106451));
#20204=CARTESIAN_POINT('Ctrl Pts',(-21.7956963171346,26.2535210123184,-45.8658996042491));
#20205=CARTESIAN_POINT('Ctrl Pts',(-21.801990469728,26.2575972746609,-45.86543870387));
#20206=CARTESIAN_POINT('Ctrl Pts',(-21.8055790202991,26.2599112063128,-45.8651759961366));
#20207=CARTESIAN_POINT('Ctrl Pts',(-21.8165165246988,26.2669330783378,-45.8643754982902));
#20208=CARTESIAN_POINT('Ctrl Pts',(-21.8238799689431,26.2716182745962,-45.8638368625392));
#20209=CARTESIAN_POINT('Ctrl Pts',(-21.8408017527841,26.2822889120907,-45.8625996375618));
#20210=CARTESIAN_POINT('Ctrl Pts',(-21.8503726200641,26.2882541807357,-45.8619003079741));
#20211=CARTESIAN_POINT('Ctrl Pts',(-21.8818567176964,26.307648677063,-45.8596011239976));
#20212=CARTESIAN_POINT('Ctrl Pts',(-21.9038988640269,26.3208657551258,-45.8579935210221));
#20213=CARTESIAN_POINT('Ctrl Pts',(-21.975021736893,26.3623645755398,-45.8528118381749));
#20214=CARTESIAN_POINT('Ctrl Pts',(-22.0246856347003,26.3896134432406,-45.8492016664255));
#20215=CARTESIAN_POINT('Ctrl Pts',(-22.0750360214967,26.415536777723,-45.8455485119974));
#20216=CARTESIAN_POINT('Origin',(-23.5502525316942,23.5502525316942,-77.3107734492734));
#20217=CARTESIAN_POINT('',(-22.0750358850059,26.4155367074495,-44.3469709746179));
#20218=CARTESIAN_POINT('',(-22.0750360439056,26.4155367892604,-44.590879968079));
#20219=CARTESIAN_POINT('',(-22.0750360153461,26.4155367745563,-77.3107734492734));
#20220=CARTESIAN_POINT('Ctrl Pts',(-22.0750358850059,26.4155367074495,-44.3469709746179));
#20221=CARTESIAN_POINT('Ctrl Pts',(-22.0169725835823,26.3856423083017,-44.3513892165499));
#20222=CARTESIAN_POINT('Ctrl Pts',(-21.9598136445485,26.3539807650537,-44.3557997793458));
#20223=CARTESIAN_POINT('Ctrl Pts',(-21.8457511816202,26.2861852140145,-44.3646822062245));
#20224=CARTESIAN_POINT('Ctrl Pts',(-21.7889519536985,26.2499698889702,-44.3691484126009));
#20225=CARTESIAN_POINT('Ctrl Pts',(-21.7045223056156,26.1923376455813,-44.3758098838951));
#20226=CARTESIAN_POINT('Ctrl Pts',(-21.6760380971063,26.1722087258025,-44.378061292946));
#20227=CARTESIAN_POINT('Ctrl Pts',(-21.6336792693039,26.1412319255837,-44.3814088395849));
#20228=CARTESIAN_POINT('Ctrl Pts',(-21.619558463127,26.1307268553778,-44.3825246902981));
#20229=CARTESIAN_POINT('Ctrl Pts',(-21.5968111644351,26.1135129116554,-44.3843211214563));
#20230=CARTESIAN_POINT('Ctrl Pts',(-21.5881317034422,26.1068750721422,-44.3850063044345));
#20231=CARTESIAN_POINT('Ctrl Pts',(-21.5775463190195,26.0986939712461,-44.3858414490104));
#20232=CARTESIAN_POINT('Ctrl Pts',(-21.5756083192604,26.0971926186904,-44.3859943289051));
#20233=CARTESIAN_POINT('Ctrl Pts',(-21.5718604427551,26.0942823203659,-44.386289938722));
#20234=CARTESIAN_POINT('Ctrl Pts',(-21.5700503541546,26.0928736515963,-44.3864326881218));
#20235=CARTESIAN_POINT('Ctrl Pts',(-21.5667712732047,26.0903161406334,-44.3866912493087));
#20236=CARTESIAN_POINT('Ctrl Pts',(-21.5653017789302,26.0891679594687,-44.3868071075507));
#20237=CARTESIAN_POINT('Ctrl Pts',(-21.5623470792556,26.0868551881438,-44.3870400345603));
#20238=CARTESIAN_POINT('Ctrl Pts',(-21.5608619062647,26.0856905735403,-44.3871571006709));
#20239=CARTESIAN_POINT('Ctrl Pts',(-21.5566207499223,26.0823588037863,-44.3874913646555));
#20240=CARTESIAN_POINT('Ctrl Pts',(-21.5538672678695,26.0801884465189,-44.3877083331261));
#20241=CARTESIAN_POINT('Ctrl Pts',(-21.542051182748,26.0708434367121,-44.3886392464672));
#20242=CARTESIAN_POINT('Ctrl Pts',(-21.5330235263869,26.0636244337569,-44.3893500499413));
#20243=CARTESIAN_POINT('Ctrl Pts',(-21.3807514102762,25.9405104582887,-44.4013358768773));
#20244=CARTESIAN_POINT('Ctrl Pts',(-21.2476429511839,25.8125696518064,-44.4117698133184));
#20245=CARTESIAN_POINT('Ctrl Pts',(-21.0203755581141,25.5531561303944,-44.4310985593496));
#20246=CARTESIAN_POINT('Ctrl Pts',(-20.9237427157361,25.4246444288825,-44.4399938590089));
#20247=CARTESIAN_POINT('Ctrl Pts',(-20.7771734304109,25.1959975505793,-44.4554736952566));
#20248=CARTESIAN_POINT('Ctrl Pts',(-20.7221314649247,25.0995013974687,-44.4619106121795));
#20249=CARTESIAN_POINT('Ctrl Pts',(-20.6499203943485,24.9561823371162,-44.4714712458676));
#20250=CARTESIAN_POINT('Ctrl Pts',(-20.6286808613619,24.9114959663492,-44.4744516673446));
#20251=CARTESIAN_POINT('Ctrl Pts',(-20.6052686809462,24.8591640967576,-44.4779475402239));
#20252=CARTESIAN_POINT('Ctrl Pts',(-20.6020845226447,24.8519762946386,-44.4784278149744));
#20253=CARTESIAN_POINT('Ctrl Pts',(-20.5972582622911,24.8409731289868,-44.4791632265973));
#20254=CARTESIAN_POINT('Ctrl Pts',(-20.5955971681179,24.837166086536,-44.4794177122683));
#20255=CARTESIAN_POINT('Ctrl Pts',(-20.5927369571064,24.8305760733751,-44.4798582961328));
#20256=CARTESIAN_POINT('Ctrl Pts',(-20.5915343940823,24.8277945965112,-44.4800442761707));
#20257=CARTESIAN_POINT('Ctrl Pts',(-20.5890508247112,24.8220278914376,-44.4804299047371));
#20258=CARTESIAN_POINT('Ctrl Pts',(-20.5877704057644,24.8190424152076,-44.4806295730832));
#20259=CARTESIAN_POINT('Ctrl Pts',(-20.5846738382919,24.8117920923489,-44.4811145368752));
#20260=CARTESIAN_POINT('Ctrl Pts',(-20.5828623768827,24.8075252621059,-44.4813999918641));
#20261=CARTESIAN_POINT('Ctrl Pts',(-20.5761212339426,24.791551025848,-44.4824688916757));
#20262=CARTESIAN_POINT('Ctrl Pts',(-20.5712516310859,24.7798185342348,-44.4832543778021));
#20263=CARTESIAN_POINT('Ctrl Pts',(-20.4912583821253,24.5838233616141,-44.4963840561369));
#20264=CARTESIAN_POINT('Ctrl Pts',(-20.4333040942262,24.3930571740781,-44.5093206099543));
#20265=CARTESIAN_POINT('Ctrl Pts',(-20.3524421671249,23.9990788085523,-44.5362338522077));
#20266=CARTESIAN_POINT('Ctrl Pts',(-20.3305052907613,23.7965474741878,-44.5501644929574));
#20267=CARTESIAN_POINT('Ctrl Pts',(-20.3267885178811,23.518331513674,-44.5686561212443));
#20268=CARTESIAN_POINT('Ctrl Pts',(-20.328403499623,23.4433422847134,-44.5735718142303));
#20269=CARTESIAN_POINT('Ctrl Pts',(-20.3343556287385,23.337986095886,-44.5803225269693));
#20270=CARTESIAN_POINT('Ctrl Pts',(-20.3365112127802,23.3075246309403,-44.5822559232885));
#20271=CARTESIAN_POINT('Ctrl Pts',(-20.3394819250748,23.272601618811,-44.5844478065109));
#20272=CARTESIAN_POINT('Ctrl Pts',(-20.3398737707547,23.2681069493158,-44.5847294365413));
#20273=CARTESIAN_POINT('Ctrl Pts',(-20.340482678102,23.2612880034529,-44.5851559737254));
#20274=CARTESIAN_POINT('Ctrl Pts',(-20.3406928264419,23.2589631393118,-44.5853012694923));
#20275=CARTESIAN_POINT('Ctrl Pts',(-20.3410594766465,23.2549554707227,-44.5855515104033));
#20276=CARTESIAN_POINT('Ctrl Pts',(-20.3412147760544,23.2532725631549,-44.5856565237815));
#20277=CARTESIAN_POINT('Ctrl Pts',(-20.3415400683596,23.2497775699289,-44.5858744689852));
#20278=CARTESIAN_POINT('Ctrl Pts',(-20.3417102720206,23.2479655109107,-44.585987388419));
#20279=CARTESIAN_POINT('Ctrl Pts',(-20.3421812947833,23.2429960245115,-44.5862968496949));
#20280=CARTESIAN_POINT('Ctrl Pts',(-20.3424852411559,23.2398388846685,-44.5864932139865));
#20281=CARTESIAN_POINT('Ctrl Pts',(-20.3436698665765,23.2277215492746,-44.5872459784305));
#20282=CARTESIAN_POINT('Ctrl Pts',(-20.3445834420388,23.2187645001618,-44.5878005351652));
#20283=CARTESIAN_POINT('Ctrl Pts',(-20.3604344347574,23.0695523827211,-44.5970090696813));
#20284=CARTESIAN_POINT('Ctrl Pts',(-20.3845284698873,22.9304021272233,-44.6051627393486));
#20285=CARTESIAN_POINT('Ctrl Pts',(-20.4611659485258,22.6132605091413,-44.6236419392076));
#20286=CARTESIAN_POINT('Ctrl Pts',(-20.5200967300328,22.4373427113619,-44.6338291931138));
#20287=CARTESIAN_POINT('Ctrl Pts',(-20.6447837179472,22.1499782549216,-44.6515709118009));
#20288=CARTESIAN_POINT('Ctrl Pts',(-20.7027093526818,22.035653608662,-44.6589470228328));
#20289=CARTESIAN_POINT('Ctrl Pts',(-20.7944915476084,21.8784836360213,-44.6697662252125));
#20290=CARTESIAN_POINT('Ctrl Pts',(-20.8228701544828,21.8325754143647,-44.6730131888152));
#20291=CARTESIAN_POINT('Ctrl Pts',(-20.8567293212722,21.7807573199098,-44.6767871793769));
#20292=CARTESIAN_POINT('Ctrl Pts',(-20.8610964573364,21.7741274810356,-44.6772721269792));
#20293=CARTESIAN_POINT('Ctrl Pts',(-20.8678233221934,21.7639969730188,-44.6780163655331));
#20294=CARTESIAN_POINT('Ctrl Pts',(-20.870165528338,21.7604846587409,-44.6782749957575));
#20295=CARTESIAN_POINT('Ctrl Pts',(-20.8742059589771,21.7544514452565,-44.6787202868754));
#20296=CARTESIAN_POINT('Ctrl Pts',(-20.8759008651161,21.7519283215563,-44.6789068221031));
#20297=CARTESIAN_POINT('Ctrl Pts',(-20.8793990565683,21.7467366182383,-44.6792912911707));
#20298=CARTESIAN_POINT('Ctrl Pts',(-20.8812027774441,21.7440683370753,-44.679489241399));
#20299=CARTESIAN_POINT('Ctrl Pts',(-20.8855552043637,21.737650459634,-44.6799662115031));
#20300=CARTESIAN_POINT('Ctrl Pts',(-20.8881078239687,21.7339035363958,-44.68024537993));
#20301=CARTESIAN_POINT('Ctrl Pts',(-20.8959675968225,21.7224185428511,-44.6811032444338));
#20302=CARTESIAN_POINT('Ctrl Pts',(-20.901300609268,21.7146983058699,-44.6816829256186));
#20303=CARTESIAN_POINT('Ctrl Pts',(-20.9211038172643,21.686296601531,-44.6838267653367));
#20304=CARTESIAN_POINT('Ctrl Pts',(-20.9357828222693,21.6657624807298,-44.6853989184963));
#20305=CARTESIAN_POINT('Ctrl Pts',(-20.9542715158919,21.6405309247524,-44.6873588722853));
#20306=CARTESIAN_POINT('Ctrl Pts',(-20.9578555196447,21.6356685608166,-44.6877378858872));
#20307=CARTESIAN_POINT('Ctrl Pts',(-20.9655423139584,21.6253011579772,-44.6885488247335));
#20308=CARTESIAN_POINT('Ctrl Pts',(-20.969649063141,21.6197991036727,-44.6889809020956));
#20309=CARTESIAN_POINT('Ctrl Pts',(-20.9746559402539,21.6131356226268,-44.6895062687476));
#20310=CARTESIAN_POINT('Ctrl Pts',(-20.9755393451414,21.6119616019797,-44.6895989104087));
#20311=CARTESIAN_POINT('Ctrl Pts',(-20.9803379865793,21.6055934094242,-44.6901018505671));
#20312=CARTESIAN_POINT('Ctrl Pts',(-20.9842681165415,21.6004105249615,-44.6905127243629));
#20313=CARTESIAN_POINT('Ctrl Pts',(-20.9938355216162,21.5878724689794,-44.6915104445947));
#20314=CARTESIAN_POINT('Ctrl Pts',(-20.9994888587572,21.5805296776051,-44.6920979084727));
#20315=CARTESIAN_POINT('Ctrl Pts',(-21.0115392127134,21.5650170510399,-44.6933457380659));
#20316=CARTESIAN_POINT('Ctrl Pts',(-21.0179441632385,21.5568535368391,-44.6940064042516));
#20317=CARTESIAN_POINT('Ctrl Pts',(-21.1655203930636,21.370617378989,-44.7091703636432));
#20318=CARTESIAN_POINT('Ctrl Pts',(-21.325072060825,21.2079681044509,-44.7244178380066));
#20319=CARTESIAN_POINT('Ctrl Pts',(-21.6011512445853,20.9803922731512,-44.7486365336156));
#20320=CARTESIAN_POINT('Ctrl Pts',(-21.7068996069316,20.9035128708808,-44.7574831994809));
#20321=CARTESIAN_POINT('Ctrl Pts',(-21.8826383657212,20.7914054261341,-44.77124045892));
#20322=CARTESIAN_POINT('Ctrl Pts',(-21.9497514008328,20.7519364721087,-44.7762909336431));
#20323=CARTESIAN_POINT('Ctrl Pts',(-22.0251503160503,20.7111958925188,-44.7816925579985));
#20324=CARTESIAN_POINT('Ctrl Pts',(-22.032080627332,20.7074839093075,-44.7821865720227));
#20325=CARTESIAN_POINT('Ctrl Pts',(-22.0441484950789,20.7010768879566,-44.7830424173952));
#20326=CARTESIAN_POINT('Ctrl Pts',(-22.0492798375856,20.6983703127437,-44.7834049562671));
#20327=CARTESIAN_POINT('Ctrl Pts',(-22.0567103316646,20.6944766381837,-44.7839279215447));
#20328=CARTESIAN_POINT('Ctrl Pts',(-22.0590036104428,20.6932784484719,-44.7840890481928));
#20329=CARTESIAN_POINT('Ctrl Pts',(-22.062984728058,20.6912044980877,-44.7843682803339));
#20330=CARTESIAN_POINT('Ctrl Pts',(-22.0646719011601,20.6903274682601,-44.7844864669854));
#20331=CARTESIAN_POINT('Ctrl Pts',(-22.067931737407,20.6886365964423,-44.7847145276506));
#20332=CARTESIAN_POINT('Ctrl Pts',(-22.0695042914533,20.6878225592538,-44.7848244142156));
#20333=CARTESIAN_POINT('Ctrl Pts',(-22.0732479999372,20.6858885283004,-44.7850857076161));
#20334=CARTESIAN_POINT('Ctrl Pts',(-22.0754197623772,20.6847697044188,-44.785237039787));
#20335=CARTESIAN_POINT('Ctrl Pts',(-22.0831141387008,20.6808168678289,-44.7857723315915));
#20336=CARTESIAN_POINT('Ctrl Pts',(-22.0886437118507,20.6779963187962,-44.7861554423007));
#20337=CARTESIAN_POINT('Ctrl Pts',(-22.1638078244865,20.6399295444725,-44.791342197598));
#20338=CARTESIAN_POINT('Ctrl Pts',(-22.2346990471095,20.6072047560611,-44.7959910189264));
#20339=CARTESIAN_POINT('Ctrl Pts',(-22.5189449489731,20.4883180115178,-44.8139564299608));
#20340=CARTESIAN_POINT('Ctrl Pts',(-22.7400850737778,20.4225240380272,-44.8265131305272));
#20341=CARTESIAN_POINT('Ctrl Pts',(-23.1511896439697,20.346787719161,-44.8500639281638));
#20342=CARTESIAN_POINT('Ctrl Pts',(-23.3386130698037,20.3289745934403,-44.86087323742));
#20343=CARTESIAN_POINT('Ctrl Pts',(-23.5397374249775,20.3274925182272,-44.8730418676754));
#20344=CARTESIAN_POINT('Ctrl Pts',(-23.5529702745348,20.3274765112967,-44.8738449734727));
#20345=CARTESIAN_POINT('Ctrl Pts',(-23.5761381853061,20.3275911762619,-44.8752555394141));
#20346=CARTESIAN_POINT('Ctrl Pts',(-23.5860733049993,20.3276862953566,-44.8758618821446));
#20347=CARTESIAN_POINT('Ctrl Pts',(-23.6005710137762,20.32789214829,-44.8767488451523));
#20348=CARTESIAN_POINT('Ctrl Pts',(-23.6051341267267,20.3279666349496,-44.8770283271636));
#20349=CARTESIAN_POINT('Ctrl Pts',(-23.6130987171833,20.328113569023,-44.8775166949268));
#20350=CARTESIAN_POINT('Ctrl Pts',(-23.616500274885,20.3281817109063,-44.8777254451794));
#20351=CARTESIAN_POINT('Ctrl Pts',(-23.6230732227454,20.3283237968118,-44.8781291624373));
#20352=CARTESIAN_POINT('Ctrl Pts',(-23.6262446256737,20.3283970372255,-44.8783241071151));
#20353=CARTESIAN_POINT('Ctrl Pts',(-23.6337659677475,20.3285818466368,-44.8787868077373));
#20354=CARTESIAN_POINT('Ctrl Pts',(-23.6381157915674,20.3286975431467,-44.8790546930827));
#20355=CARTESIAN_POINT('Ctrl Pts',(-23.6511131829695,20.3290695909416,-44.8798560196478));
#20356=CARTESIAN_POINT('Ctrl Pts',(-23.6597599143415,20.3293519527296,-44.8803902770197));
#20357=CARTESIAN_POINT('Ctrl Pts',(-23.7419484046763,20.3323671830337,-44.8854796878124));
#20358=CARTESIAN_POINT('Ctrl Pts',(-23.8153720750082,20.3375832969437,-44.8901124887298));
#20359=CARTESIAN_POINT('Ctrl Pts',(-23.9282473178351,20.3494977651845,-44.8973765586769));
#20360=CARTESIAN_POINT('Ctrl Pts',(-23.9678636276213,20.3544252694393,-44.8999530840359));
#20361=CARTESIAN_POINT('Ctrl Pts',(-24.3032778109199,20.4024873528457,-44.9219952892521));
#20362=CARTESIAN_POINT('Ctrl Pts',(-24.591830282267,20.4858535029736,-44.9426587130554));
#20363=CARTESIAN_POINT('Ctrl Pts',(-24.9293705036529,20.6366345390483,-44.967181020467));
#20364=CARTESIAN_POINT('Ctrl Pts',(-24.9930874681241,20.6676555986252,-44.971816987828));
#20365=CARTESIAN_POINT('Ctrl Pts',(-25.0818483779472,20.7145508534923,-44.9782345107791));
#20366=CARTESIAN_POINT('Ctrl Pts',(-25.1077724517435,20.7287065555354,-44.9801037353328));
#20367=CARTESIAN_POINT('Ctrl Pts',(-25.1373969822194,20.7454156237942,-44.9822306440995));
#20368=CARTESIAN_POINT('Ctrl Pts',(-25.1412900464867,20.7476221219093,-44.9825099651054));
#20369=CARTESIAN_POINT('Ctrl Pts',(-25.1472002051788,20.7509881455452,-44.9829337150519));
#20370=CARTESIAN_POINT('Ctrl Pts',(-25.1492206403128,20.7521417470552,-44.9830785249679));
#20371=CARTESIAN_POINT('Ctrl Pts',(-25.1528601753934,20.7542250302901,-44.9833392830459));
#20372=CARTESIAN_POINT('Ctrl Pts',(-25.1544797128154,20.7551539288429,-44.9834552815724));
#20373=CARTESIAN_POINT('Ctrl Pts',(-25.1577186438274,20.7570153858573,-44.9836871982694));
#20374=CARTESIAN_POINT('Ctrl Pts',(-25.1593380270245,20.7579479417004,-44.9838031158737));
#20375=CARTESIAN_POINT('Ctrl Pts',(-25.1639132901304,20.7605880049193,-44.9841305233886));
#20376=CARTESIAN_POINT('Ctrl Pts',(-25.166867280788,20.7622988074491,-44.9843417987758));
#20377=CARTESIAN_POINT('Ctrl Pts',(-25.1791574988787,20.7694427837216,-44.9852203717435));
#20378=CARTESIAN_POINT('Ctrl Pts',(-25.1884692386814,20.7749182679858,-44.9858849476514));
#20379=CARTESIAN_POINT('Ctrl Pts',(-25.31484519532,20.8500874505381,-44.9948921019625));
#20380=CARTESIAN_POINT('Ctrl Pts',(-25.4274194536192,20.9270992391841,-45.0027740407067));
#20381=CARTESIAN_POINT('Ctrl Pts',(-25.5948174109338,21.0579291798846,-45.0148168165361));
#20382=CARTESIAN_POINT('Ctrl Pts',(-25.6531609486468,21.1069559954136,-45.0190814707401));
#20383=CARTESIAN_POINT('Ctrl Pts',(-25.8296936744641,21.2663105592593,-45.0323746359616));
#20384=CARTESIAN_POINT('Ctrl Pts',(-25.941352421998,21.3834852286414,-45.0413739313162));
#20385=CARTESIAN_POINT('Ctrl Pts',(-26.1243003304545,21.6069143806605,-45.0579921632987));
#20386=CARTESIAN_POINT('Ctrl Pts',(-26.1989534783728,21.709963835474,-45.0654782918616));
#20387=CARTESIAN_POINT('Ctrl Pts',(-26.273361661736,21.8266167067517,-45.0738952107026));
#20388=CARTESIAN_POINT('Ctrl Pts',(-26.2793539880419,21.8361203818638,-45.0745804866644));
#20389=CARTESIAN_POINT('Ctrl Pts',(-26.2878108739276,21.8496895412562,-45.0755583473319));
#20390=CARTESIAN_POINT('Ctrl Pts',(-26.2903163693343,21.8537295206943,-45.0758494175754));
#20391=CARTESIAN_POINT('Ctrl Pts',(-26.2946172525071,21.8606988491651,-45.0763514246348));
#20392=CARTESIAN_POINT('Ctrl Pts',(-26.2964169164785,21.8636255609076,-45.0765622034144));
#20393=CARTESIAN_POINT('Ctrl Pts',(-26.2998464221396,21.86922285066,-45.076965250311));
#20394=CARTESIAN_POINT('Ctrl Pts',(-26.3014770628597,21.8718929367649,-45.0771574887376));
#20395=CARTESIAN_POINT('Ctrl Pts',(-26.3052767833891,21.8781351911929,-45.077606850173));
#20396=CARTESIAN_POINT('Ctrl Pts',(-26.3074428045839,21.881709206917,-45.0778640851357));
#20397=CARTESIAN_POINT('Ctrl Pts',(-26.314862400078,21.894005714278,-45.0787489529087));
#20398=CARTESIAN_POINT('Ctrl Pts',(-26.3200815427048,21.9027488168243,-45.0793778442057));
#20399=CARTESIAN_POINT('Ctrl Pts',(-26.3741684089553,21.9943385544905,-45.0859633831031));
#20400=CARTESIAN_POINT('Ctrl Pts',(-26.4193406353654,22.0793006466735,-45.0920532553449));
#20401=CARTESIAN_POINT('Ctrl Pts',(-26.5610097665651,22.3771918997081,-45.113373878517));
#20402=CARTESIAN_POINT('Ctrl Pts',(-26.6381112326239,22.5985017357892,-45.1292230096892));
#20403=CARTESIAN_POINT('Ctrl Pts',(-26.7295860685309,22.995222832459,-45.1567407211548));
#20404=CARTESIAN_POINT('Ctrl Pts',(-26.754857500866,23.1671823410113,-45.1683685278468));
#20405=CARTESIAN_POINT('Ctrl Pts',(-26.7668434730624,23.3508275649975,-45.1799527221918));
#20406=CARTESIAN_POINT('Ctrl Pts',(-26.7674755659971,23.3612986848333,-45.180610329277));
#20407=CARTESIAN_POINT('Ctrl Pts',(-26.7682361194059,23.3750106778657,-45.1814675057145));
#20408=CARTESIAN_POINT('Ctrl Pts',(-26.768410822246,23.3782487663602,-45.1816696387536));
#20409=CARTESIAN_POINT('Ctrl Pts',(-26.7686873488845,23.3835220833069,-45.1819983409278));
#20410=CARTESIAN_POINT('Ctrl Pts',(-26.7687921297576,23.3855571441588,-45.1821250768914));
#20411=CARTESIAN_POINT('Ctrl Pts',(-26.7689904254819,23.3894809248369,-45.1823692104319));
#20412=CARTESIAN_POINT('Ctrl Pts',(-26.7690842078933,23.3913696226442,-45.1824866226049));
#20413=CARTESIAN_POINT('Ctrl Pts',(-26.7692971605752,23.3957358908377,-45.18275782381));
#20414=CARTESIAN_POINT('Ctrl Pts',(-26.7694151332441,23.398213523834,-45.1829115448948));
#20415=CARTESIAN_POINT('Ctrl Pts',(-26.7697753407421,23.4059669233087,-45.1833920628319));
#20416=CARTESIAN_POINT('Ctrl Pts',(-26.7700074691429,23.4112431849558,-45.1837182916079));
#20417=CARTESIAN_POINT('Ctrl Pts',(-26.7719120699812,23.4571016385121,-45.1865472069361));
#20418=CARTESIAN_POINT('Ctrl Pts',(-26.7728302773295,23.4977137980555,-45.1890083205923));
#20419=CARTESIAN_POINT('Ctrl Pts',(-26.7729937518526,23.5419194276276,-45.1916496469392));
#20420=CARTESIAN_POINT('Ctrl Pts',(-26.7730010272996,23.5455041604006,-45.1918635692455));
#20421=CARTESIAN_POINT('Ctrl Pts',(-26.7730321986284,23.6318360839317,-45.1970091952331));
#20422=CARTESIAN_POINT('Ctrl Pts',(-26.7698751374493,23.7145601871732,-45.2018004724637));
#20423=CARTESIAN_POINT('Ctrl Pts',(-26.7412431602374,24.0873058694652,-45.2231168771338));
#20424=CARTESIAN_POINT('Ctrl Pts',(-26.6797358568846,24.3731690499141,-45.2388484144448));
#20425=CARTESIAN_POINT('Ctrl Pts',(-26.5492046359256,24.733873763714,-45.2612377452138));
#20426=CARTESIAN_POINT('Ctrl Pts',(-26.5140030105104,24.8194465797843,-45.2667391947205));
#20427=CARTESIAN_POINT('Ctrl Pts',(-26.4708835928088,24.9126534019564,-45.2729909010341));
#20428=CARTESIAN_POINT('Ctrl Pts',(-26.4665502562231,24.9219046393978,-45.2736142978734));
#20429=CARTESIAN_POINT('Ctrl Pts',(-26.4604096853497,24.9348534994649,-45.2744909679228));
#20430=CARTESIAN_POINT('Ctrl Pts',(-26.4586392109606,24.9385685701141,-45.2747429637209));
#20431=CARTESIAN_POINT('Ctrl Pts',(-26.455382404655,24.9453689110046,-45.2752051131632));
#20432=CARTESIAN_POINT('Ctrl Pts',(-26.4538982594631,24.9484552273224,-45.2754151904567));
#20433=CARTESIAN_POINT('Ctrl Pts',(-26.450884980503,24.9546959260041,-45.2758406531165));
#20434=CARTESIAN_POINT('Ctrl Pts',(-26.4493556142839,24.9578501898577,-45.2760560463556));
#20435=CARTESIAN_POINT('Ctrl Pts',(-26.4455858950721,24.965592897282,-45.2765856309788));
#20436=CARTESIAN_POINT('Ctrl Pts',(-26.4433397831903,24.9701785122659,-45.2769000233911));
#20437=CARTESIAN_POINT('Ctrl Pts',(-26.4351547041232,24.9867889517107,-45.2780415681139));
#20438=CARTESIAN_POINT('Ctrl Pts',(-26.4291516508244,24.99878188371,-45.2788709642983));
#20439=CARTESIAN_POINT('Ctrl Pts',(-26.3409887841099,25.17220118813,-45.2909405528309));
#20440=CARTESIAN_POINT('Ctrl Pts',(-26.2454526735476,25.3264288107428,-45.3026669017893));
#20441=CARTESIAN_POINT('Ctrl Pts',(-25.966591284306,25.7018975621877,-45.3338298404498));
#20442=CARTESIAN_POINT('Ctrl Pts',(-25.765773544799,25.9081609206969,-45.353719126118));
#20443=CARTESIAN_POINT('Ctrl Pts',(-25.5100472888222,26.1089249714982,-45.3746414491687));
#20444=CARTESIAN_POINT('Ctrl Pts',(-25.4793358311925,26.1321584356106,-45.3770892641025));
#20445=CARTESIAN_POINT('Ctrl Pts',(-25.4443795213895,26.1576311034743,-45.3797966903431));
#20446=CARTESIAN_POINT('Ctrl Pts',(-25.4405391491752,26.1604166211963,-45.3800930837598));
#20447=CARTESIAN_POINT('Ctrl Pts',(-25.4347442032644,26.1646003427752,-45.380538730874));
#20448=CARTESIAN_POINT('Ctrl Pts',(-25.4327942150391,26.1660048418496,-45.3806884187287));
#20449=CARTESIAN_POINT('Ctrl Pts',(-25.4294130743251,26.168434403992,-45.380947494078));
#20450=CARTESIAN_POINT('Ctrl Pts',(-25.4279826531968,26.169460475376,-45.3810569518733));
#20451=CARTESIAN_POINT('Ctrl Pts',(-25.4249992995014,26.1715967981597,-45.3812849361929));
#20452=CARTESIAN_POINT('Ctrl Pts',(-25.4234462227242,26.172706840665,-45.3814034477518));
#20453=CARTESIAN_POINT('Ctrl Pts',(-25.4197512798437,26.175342798552,-45.3816849917962));
#20454=CARTESIAN_POINT('Ctrl Pts',(-25.4176085242473,26.1768674779089,-45.381847938076));
#20455=CARTESIAN_POINT('Ctrl Pts',(-25.4104402114887,26.181954890924,-45.3823919754168));
#20456=CARTESIAN_POINT('Ctrl Pts',(-25.4054062658167,26.185505865985,-45.3827722566296));
#20457=CARTESIAN_POINT('Ctrl Pts',(-25.2571892209753,26.2894238691042,-45.3939181881737));
#20458=CARTESIAN_POINT('Ctrl Pts',(-25.1060592960262,26.3780038839481,-45.4038974436268));
#20459=CARTESIAN_POINT('Ctrl Pts',(-24.7383053689803,26.5550913930487,-45.426839197013));
#20460=CARTESIAN_POINT('Ctrl Pts',(-24.517793410645,26.6331710177218,-45.4396595269493));
#20461=CARTESIAN_POINT('Ctrl Pts',(-24.1927260648965,26.7099198296471,-45.4590857302529));
#20462=CARTESIAN_POINT('Ctrl Pts',(-24.0936416790154,26.7284587416941,-45.465064435559));
#20463=CARTESIAN_POINT('Ctrl Pts',(-23.9845534767991,26.7436188609489,-45.4717679415841));
#20464=CARTESIAN_POINT('Ctrl Pts',(-23.9752426270166,26.7448713258039,-45.4723410307475));
#20465=CARTESIAN_POINT('Ctrl Pts',(-23.9614277581929,26.746668192521,-45.473192774146));
#20466=CARTESIAN_POINT('Ctrl Pts',(-23.9569277935016,26.7472438320822,-45.4734704399695));
#20467=CARTESIAN_POINT('Ctrl Pts',(-23.9492303195171,26.748211985072,-45.4739457941239));
#20468=CARTESIAN_POINT('Ctrl Pts',(-23.946033400301,26.7486092104523,-45.4741433332132));
#20469=CARTESIAN_POINT('Ctrl Pts',(-23.9398192647578,26.7493718730358,-45.4745275325132));
#20470=CARTESIAN_POINT('Ctrl Pts',(-23.9368021160454,26.7497378369264,-45.4747141758154));
#20471=CARTESIAN_POINT('Ctrl Pts',(-23.9296790025828,26.7505916094527,-45.4751550627587));
#20472=CARTESIAN_POINT('Ctrl Pts',(-23.925572615267,26.7510757842419,-45.4754094209627));
#20473=CARTESIAN_POINT('Ctrl Pts',(-23.9134349872087,26.7524832260508,-45.4761618254598));
#20474=CARTESIAN_POINT('Ctrl Pts',(-23.9054012356492,26.7533841730794,-45.4766605760629));
#20475=CARTESIAN_POINT('Ctrl Pts',(-23.8871626850371,26.7553600812507,-45.4777945794142));
#20476=CARTESIAN_POINT('Ctrl Pts',(-23.8769560087251,26.7564165464982,-45.4784304118783));
#20477=CARTESIAN_POINT('Ctrl Pts',(-23.7882252624795,26.7651727267044,-45.4839687965563));
#20478=CARTESIAN_POINT('Ctrl Pts',(-23.7094540852722,26.7700345088245,-45.4889602488078));
#20479=CARTESIAN_POINT('Ctrl Pts',(-23.5553034239995,26.7738783643619,-45.4988844937393));
#20480=CARTESIAN_POINT('Ctrl Pts',(-23.4799799534304,26.7731160778694,-45.5038065085097));
#20481=CARTESIAN_POINT('Ctrl Pts',(-23.1046353526768,26.7561532812966,-45.5286669960293));
#20482=CARTESIAN_POINT('Ctrl Pts',(-22.8079168428669,26.7006958470769,-45.5495584711883));
#20483=CARTESIAN_POINT('Ctrl Pts',(-22.5191689055393,26.603611675694,-45.5692877037621));
#20484=CARTESIAN_POINT('Ctrl Pts',(-22.5151564042361,26.6022537626356,-45.5695617087534));
#20485=CARTESIAN_POINT('Ctrl Pts',(-22.5054210655288,26.5989377162579,-45.5702261145347));
#20486=CARTESIAN_POINT('Ctrl Pts',(-22.499701017421,26.5969713674669,-45.5706161539965));
#20487=CARTESIAN_POINT('Ctrl Pts',(-22.4574010109084,26.5822968424369,-45.5734978561477));
#20488=CARTESIAN_POINT('Ctrl Pts',(-22.4210451807522,26.5689456664167,-45.5759599067181));
#20489=CARTESIAN_POINT('Ctrl Pts',(-22.3805065096659,26.5532234584556,-45.5786816308035));
#20490=CARTESIAN_POINT('Ctrl Pts',(-22.3760799120296,26.551495408061,-45.5789785090993));
#20491=CARTESIAN_POINT('Ctrl Pts',(-22.3694186275566,26.5488779897712,-45.5794247626371));
#20492=CARTESIAN_POINT('Ctrl Pts',(-22.3671811123695,26.5479959102805,-45.5795745736815));
#20493=CARTESIAN_POINT('Ctrl Pts',(-22.3633071232243,26.5464636825496,-45.5798338038848));
#20494=CARTESIAN_POINT('Ctrl Pts',(-22.3616701949922,26.5458146979849,-45.5799432935444));
#20495=CARTESIAN_POINT('Ctrl Pts',(-22.3582601318707,26.5444594924763,-45.5801712855241));
#20496=CARTESIAN_POINT('Ctrl Pts',(-22.3564870942583,26.5437530387319,-45.5802897729619));
#20497=CARTESIAN_POINT('Ctrl Pts',(-22.3522745330482,26.5420702369977,-45.5805711579638));
#20498=CARTESIAN_POINT('Ctrl Pts',(-22.3498355668013,26.5410924768471,-45.5807339695857));
#20499=CARTESIAN_POINT('Ctrl Pts',(-22.3416942815873,26.5378171441703,-45.5812770998512));
#20500=CARTESIAN_POINT('Ctrl Pts',(-22.3359972963003,26.5355062198109,-45.5816566123466));
#20501=CARTESIAN_POINT('Ctrl Pts',(-22.2435254400753,26.4976874406595,-45.5878083317032));
#20502=CARTESIAN_POINT('Ctrl Pts',(-22.158354761156,26.4584341573107,-45.5933540196748));
#20503=CARTESIAN_POINT('Ctrl Pts',(-22.075035968613,26.4155367504953,-45.5987738960335));
#20504=CARTESIAN_POINT('',(-26.7730015954251,23.5477959646253,-45.4377814573121));
#20505=CARTESIAN_POINT('Ctrl Pts',(-22.0750360214967,26.415536777723,-45.8455485119974));
#20506=CARTESIAN_POINT('Ctrl Pts',(-22.0932331211949,26.4249057127422,-45.844228227893));
#20507=CARTESIAN_POINT('Ctrl Pts',(-22.1115198899388,26.4341015112559,-45.842902360652));
#20508=CARTESIAN_POINT('Ctrl Pts',(-22.2339163535886,26.4941964530481,-45.8340345953022));
#20509=CARTESIAN_POINT('Ctrl Pts',(-22.3406090816023,26.5396179041769,-45.8263310922209));
#20510=CARTESIAN_POINT('Ctrl Pts',(-22.6831170533065,26.6640884797216,-45.8018196283623));
#20511=CARTESIAN_POINT('Ctrl Pts',(-22.9257694193826,26.721676500522,-45.7847079721004));
#20512=CARTESIAN_POINT('Ctrl Pts',(-23.2067875505152,26.7548323662921,-45.766549079901));
#20513=CARTESIAN_POINT('Ctrl Pts',(-23.2410029016038,26.7583150331222,-45.7643669235498));
#20514=CARTESIAN_POINT('Ctrl Pts',(-23.2798433131508,26.7616412490265,-45.7619273093996));
#20515=CARTESIAN_POINT('Ctrl Pts',(-23.2844183817378,26.7620232029315,-45.7616405328371));
#20516=CARTESIAN_POINT('Ctrl Pts',(-23.2913503768492,26.7625870137509,-45.7612069266999));
#20517=CARTESIAN_POINT('Ctrl Pts',(-23.2937066886552,26.7627760539274,-45.7610596949936));
#20518=CARTESIAN_POINT('Ctrl Pts',(-23.2978081927628,26.7631005645538,-45.7608036958914));
#20519=CARTESIAN_POINT('Ctrl Pts',(-23.2995532872719,26.7632372056989,-45.7606948621655));
#20520=CARTESIAN_POINT('Ctrl Pts',(-23.303210314001,26.7635205538429,-45.7604669752774));
#20521=CARTESIAN_POINT('Ctrl Pts',(-23.3051222650122,26.7636669761543,-45.7603479387869));
#20522=CARTESIAN_POINT('Ctrl Pts',(-23.3097025030671,26.7640136314109,-45.7600630293673));
#20523=CARTESIAN_POINT('Ctrl Pts',(-23.3123709190455,26.7642122484319,-45.759897248194));
#20524=CARTESIAN_POINT('Ctrl Pts',(-23.3214496065645,26.7648766298269,-45.7593339033445));
#20525=CARTESIAN_POINT('Ctrl Pts',(-23.3278610764336,26.7653265453296,-45.7589372303916));
#20526=CARTESIAN_POINT('Ctrl Pts',(-23.3431220310402,26.7663515912021,-45.7579957329688));
#20527=CARTESIAN_POINT('Ctrl Pts',(-23.3519726821841,26.766909384762,-45.7574518565877));
#20528=CARTESIAN_POINT('Ctrl Pts',(-23.4570304964405,26.7730951706566,-45.7510203094309));
#20529=CARTESIAN_POINT('Ctrl Pts',(-23.5534516378947,26.774442160417,-45.7453588402578));
#20530=CARTESIAN_POINT('Ctrl Pts',(-23.7338978176656,26.7688658280046,-45.7349773740592));
#20531=CARTESIAN_POINT('Ctrl Pts',(-23.8178675640792,26.7629742023149,-45.7302331595992));
#20532=CARTESIAN_POINT('Ctrl Pts',(-23.922031018559,26.7515529463684,-45.7243589640467));
#20533=CARTESIAN_POINT('Ctrl Pts',(-23.9425264350419,26.7491061981499,-45.7232037150364));
#20534=CARTESIAN_POINT('Ctrl Pts',(-23.9808183542393,26.7441613487728,-45.7210444092883));
#20535=CARTESIAN_POINT('Ctrl Pts',(-23.9986201701884,26.7417109634887,-45.7200401745927));
#20536=CARTESIAN_POINT('Ctrl Pts',(-24.1716457302892,26.7164180545362,-45.7102691335204));
#20537=CARTESIAN_POINT('Ctrl Pts',(-24.3250206543941,26.6824185730999,-45.7015139056533));
#20538=CARTESIAN_POINT('Ctrl Pts',(-24.5123817935236,26.626276464297,-45.6902377880939));
#20539=CARTESIAN_POINT('Ctrl Pts',(-24.5492576995849,26.614498681982,-45.6879902703741));
#20540=CARTESIAN_POINT('Ctrl Pts',(-24.6056888843577,26.5953482370758,-45.684501095138));
#20541=CARTESIAN_POINT('Ctrl Pts',(-24.6254001475624,26.5884446464585,-45.683272872589));
#20542=CARTESIAN_POINT('Ctrl Pts',(-24.7066383600016,26.5591025390506,-45.6781693273891));
#20543=CARTESIAN_POINT('Ctrl Pts',(-24.7675379578507,26.5349839785283,-45.6742439646287));
#20544=CARTESIAN_POINT('Ctrl Pts',(-24.8353415429127,26.5057108457034,-45.6697452134095));
#20545=CARTESIAN_POINT('Ctrl Pts',(-24.8430125762614,26.5023634845028,-45.6692343661572));
#20546=CARTESIAN_POINT('Ctrl Pts',(-24.8545861024484,26.4972594562234,-45.6684607635568));
#20547=CARTESIAN_POINT('Ctrl Pts',(-24.8584983195285,26.4955248171282,-45.6681987638727));
#20548=CARTESIAN_POINT('Ctrl Pts',(-24.8652876788679,26.4924982847094,-45.6677432134642));
#20549=CARTESIAN_POINT('Ctrl Pts',(-24.8681664084323,26.4912099477123,-45.667549785173));
#20550=CARTESIAN_POINT('Ctrl Pts',(-24.8739561675086,26.4886086103741,-45.6671602081692));
#20551=CARTESIAN_POINT('Ctrl Pts',(-24.8768671452372,26.487295505095,-45.6669640560323));
#20552=CARTESIAN_POINT('Ctrl Pts',(-24.8828026564844,26.4846074464491,-45.6665635253163));
#20553=CARTESIAN_POINT('Ctrl Pts',(-24.8858270242565,26.4832321387678,-45.666359134698));
#20554=CARTESIAN_POINT('Ctrl Pts',(-24.8957997353745,26.4786785025035,-45.6656841552503));
#20555=CARTESIAN_POINT('Ctrl Pts',(-24.90273886281,26.475480158115,-45.6652128751468));
#20556=CARTESIAN_POINT('Ctrl Pts',(-24.9494907823421,26.4537296066758,-45.6620266090919));
#20557=CARTESIAN_POINT('Ctrl Pts',(-24.9889304379036,26.4343905972579,-45.6592844124577));
#20558=CARTESIAN_POINT('Ctrl Pts',(-25.0907383523097,26.3818618156891,-45.6520583963383));
#20559=CARTESIAN_POINT('Ctrl Pts',(-25.1524294724456,26.3474181539741,-45.647531596187));
#20560=CARTESIAN_POINT('Ctrl Pts',(-25.2732667424991,26.2746423150326,-45.6383623908322));
#20561=CARTESIAN_POINT('Ctrl Pts',(-25.3323872803082,26.2363412085222,-45.6337228315378));
#20562=CARTESIAN_POINT('Ctrl Pts',(-25.6491876305378,26.0160379113047,-45.608043033346));
#20563=CARTESIAN_POINT('Ctrl Pts',(-25.8803149713862,25.7989036534411,-45.5860397343649));
#20564=CARTESIAN_POINT('Ctrl Pts',(-26.0863683622212,25.5388453539497,-45.5650390869338));
#20565=CARTESIAN_POINT('Ctrl Pts',(-26.0964253369512,25.525952152405,-45.5640104329362));
#20566=CARTESIAN_POINT('Ctrl Pts',(-26.1085750182408,25.5101292012963,-45.5627637979426));
#20567=CARTESIAN_POINT('Ctrl Pts',(-26.1107612739811,25.5072720732943,-45.5625393165491));
#20568=CARTESIAN_POINT('Ctrl Pts',(-26.1143548544824,25.5025594399686,-45.5621700814502));
#20569=CARTESIAN_POINT('Ctrl Pts',(-26.1157649524785,25.5007060698993,-45.5620251317832));
#20570=CARTESIAN_POINT('Ctrl Pts',(-26.1183020772094,25.4973638744345,-45.5617642171858));
#20571=CARTESIAN_POINT('Ctrl Pts',(-26.119429816298,25.4958756014545,-45.5616482016347));
#20572=CARTESIAN_POINT('Ctrl Pts',(-26.1218501747177,25.4926756898648,-45.5613991221658));
#20573=CARTESIAN_POINT('Ctrl Pts',(-26.1231423753933,25.4909637454651,-45.5612660881557));
#20574=CARTESIAN_POINT('Ctrl Pts',(-26.126671982098,25.4862779003522,-45.5609025595889));
#20575=CARTESIAN_POINT('Ctrl Pts',(-26.1289059563282,25.4833014003113,-45.5606723079115));
#20576=CARTESIAN_POINT('Ctrl Pts',(-26.1404167126564,25.4679092487397,-45.5594850196444));
#20577=CARTESIAN_POINT('Ctrl Pts',(-26.1496092068731,25.455430388674,-45.5585338367919));
#20578=CARTESIAN_POINT('Ctrl Pts',(-26.203298951527,25.3814342640725,-45.5529572330896));
#20579=CARTESIAN_POINT('Ctrl Pts',(-26.2457049345611,25.3184211395376,-45.5484657394944));
#20580=CARTESIAN_POINT('Ctrl Pts',(-26.4308887957867,25.0210771098771,-45.528142400024));
#20581=CARTESIAN_POINT('Ctrl Pts',(-26.5456049614685,24.7706123587006,-45.5133402523503));
#20582=CARTESIAN_POINT('Ctrl Pts',(-26.6329142654349,24.4902965054614,-45.4965542690082));
#20583=CARTESIAN_POINT('Ctrl Pts',(-26.6384586989395,24.4719187889303,-45.4954533287968));
#20584=CARTESIAN_POINT('Ctrl Pts',(-26.6495809833839,24.4338251126536,-45.4931692212223));
#20585=CARTESIAN_POINT('Ctrl Pts',(-26.6551356407016,24.414103337585,-45.4919855662485));
#20586=CARTESIAN_POINT('Ctrl Pts',(-26.6698105997036,24.3600291893616,-45.4887353545723));
#20587=CARTESIAN_POINT('Ctrl Pts',(-26.6785510956958,24.3255774583779,-45.4866592760994));
#20588=CARTESIAN_POINT('Ctrl Pts',(-26.6900987965241,24.2766815496717,-45.4837012043833));
#20589=CARTESIAN_POINT('Ctrl Pts',(-26.6933798102469,24.2623512509855,-45.4828328691964));
#20590=CARTESIAN_POINT('Ctrl Pts',(-26.6974694769903,24.243909944142,-45.4817134125032));
#20591=CARTESIAN_POINT('Ctrl Pts',(-26.6983683536607,24.239818973637,-45.4814649480156));
#20592=CARTESIAN_POINT('Ctrl Pts',(-26.7000677915748,24.2320119037782,-45.4809905366412));
#20593=CARTESIAN_POINT('Ctrl Pts',(-26.7008697587294,24.2282961153476,-45.4807646317626));
#20594=CARTESIAN_POINT('Ctrl Pts',(-26.7031012567801,24.2178673806173,-45.4801302959796));
#20595=CARTESIAN_POINT('Ctrl Pts',(-26.7045159141957,24.2111513004468,-45.4797214240073));
#20596=CARTESIAN_POINT('Ctrl Pts',(-26.7076882272467,24.1958485440645,-45.478788939057));
#20597=CARTESIAN_POINT('Ctrl Pts',(-26.7094323243651,24.1872591392677,-45.4782649216822));
#20598=CARTESIAN_POINT('Ctrl Pts',(-26.7126900963205,24.1708726229237,-45.4772639872759));
#20599=CARTESIAN_POINT('Ctrl Pts',(-26.714210029584,24.1630768112884,-45.4767872654356));
#20600=CARTESIAN_POINT('Ctrl Pts',(-26.7200551394064,24.1324955024424,-45.474915012691));
#20601=CARTESIAN_POINT('Ctrl Pts',(-26.7241630405492,24.1096696279425,-45.4735128309974));
#20602=CARTESIAN_POINT('Ctrl Pts',(-26.7299914343831,24.0751503325694,-45.47138441366));
#20603=CARTESIAN_POINT('Ctrl Pts',(-26.7318946120283,24.0634882060678,-45.4706639840158));
#20604=CARTESIAN_POINT('Ctrl Pts',(-26.734433217846,24.0473753826809,-45.4696666576261));
#20605=CARTESIAN_POINT('Ctrl Pts',(-26.7351235502036,24.0429333270995,-45.4693915055423));
#20606=CARTESIAN_POINT('Ctrl Pts',(-26.7362909637467,24.0353164236135,-45.4689193394605));
#20607=CARTESIAN_POINT('Ctrl Pts',(-26.736772600416,24.0321422714484,-45.4687224702966));
#20608=CARTESIAN_POINT('Ctrl Pts',(-26.737729484473,24.0257719105155,-45.4683271494224));
#20609=CARTESIAN_POINT('Ctrl Pts',(-26.7382046693119,24.0225756967735,-45.4681286960091));
#20610=CARTESIAN_POINT('Ctrl Pts',(-26.7391520762268,24.0161366336653,-45.4677286733704));
#20611=CARTESIAN_POINT('Ctrl Pts',(-26.7396241606454,24.0128937684043,-45.4675271000424));
#20612=CARTESIAN_POINT('Ctrl Pts',(-26.7406935169153,24.0054686673828,-45.4670653033087));
#20613=CARTESIAN_POINT('Ctrl Pts',(-26.7412875119866,24.0012859724142,-45.4668049762491));
#20614=CARTESIAN_POINT('Ctrl Pts',(-26.7427852061509,23.9905887004333,-45.4661387004403));
#20615=CARTESIAN_POINT('Ctrl Pts',(-26.7436771871845,23.9840725262204,-45.4657323808035));
#20616=CARTESIAN_POINT('Ctrl Pts',(-26.7455910060445,23.9697657430924,-45.4648392427615));
#20617=CARTESIAN_POINT('Ctrl Pts',(-26.746604309516,23.9619740526951,-45.4643521562291));
#20618=CARTESIAN_POINT('Ctrl Pts',(-26.7646199230559,23.8193688646117,-45.4554249193446));
#20619=CARTESIAN_POINT('Ctrl Pts',(-26.7731051425797,23.683638580119,-45.446715141092));
#20620=CARTESIAN_POINT('Ctrl Pts',(-26.7730015954251,23.5477959646253,-45.4377814573121));
#20621=CARTESIAN_POINT('Ctrl Pts',(-26.7730015985351,23.5478000480778,-45.4377817258601));
#20622=CARTESIAN_POINT('Ctrl Pts',(-26.7728034974816,23.2874802721333,-45.4206618149297));
#20623=CARTESIAN_POINT('Ctrl Pts',(-26.7410675662046,23.0281666471294,-45.4027352975828));
#20624=CARTESIAN_POINT('Ctrl Pts',(-26.6551711849931,22.6813409747046,-45.3789621655378));
#20625=CARTESIAN_POINT('Ctrl Pts',(-26.6276096000244,22.5882729779119,-45.3726171768751));
#20626=CARTESIAN_POINT('Ctrl Pts',(-26.592978418147,22.488171587896,-45.3659313184682));
#20627=CARTESIAN_POINT('Ctrl Pts',(-26.5900341125884,22.4797738088478,-45.3653715175065));
#20628=CARTESIAN_POINT('Ctrl Pts',(-26.5848975046335,22.4653152123082,-45.3644097197638));
#20629=CARTESIAN_POINT('Ctrl Pts',(-26.5827217540219,22.4592486288017,-45.3640067812941));
#20630=CARTESIAN_POINT('Ctrl Pts',(-26.5796159063412,22.4506697550354,-45.3634378921017));
#20631=CARTESIAN_POINT('Ctrl Pts',(-26.5787008714247,22.4481520861421,-45.3632710500649));
#20632=CARTESIAN_POINT('Ctrl Pts',(-26.5771252521819,22.4438336347131,-45.3629850682525));
#20633=CARTESIAN_POINT('Ctrl Pts',(-26.5764661984156,22.4420322985958,-45.3628658363443));
#20634=CARTESIAN_POINT('Ctrl Pts',(-26.5752028406082,22.4385887997385,-45.3626380214458));
#20635=CARTESIAN_POINT('Ctrl Pts',(-26.574598808126,22.4369465429322,-45.3625294221929));
#20636=CARTESIAN_POINT('Ctrl Pts',(-26.5731764772806,22.4330891783799,-45.362274455812));
#20637=CARTESIAN_POINT('Ctrl Pts',(-26.5723570798476,22.4308744727247,-45.3621281549943));
#20638=CARTESIAN_POINT('Ctrl Pts',(-26.5699407981392,22.424365625477,-45.3616984419026));
#20639=CARTESIAN_POINT('Ctrl Pts',(-26.5683371818847,22.4200739630624,-45.3614154318165));
#20640=CARTESIAN_POINT('Ctrl Pts',(-26.5547035375743,22.3838230092142,-45.3590275238853));
#20641=CARTESIAN_POINT('Ctrl Pts',(-26.542174819467,22.3520518266533,-45.356952007745));
#20642=CARTESIAN_POINT('Ctrl Pts',(-26.4113695088488,22.0351997138116,-45.3363702189845));
#20643=CARTESIAN_POINT('Ctrl Pts',(-26.2532097011805,21.7682703403302,-45.31986470917));
#20644=CARTESIAN_POINT('Ctrl Pts',(-26.0298486387752,21.4911390425142,-45.2996459172125));
#20645=CARTESIAN_POINT('Ctrl Pts',(-25.9994276656126,21.4550470164918,-45.2969468322258));
#20646=CARTESIAN_POINT('Ctrl Pts',(-25.9137067431168,21.3577648475905,-45.2894640793166));
#20647=CARTESIAN_POINT('Ctrl Pts',(-25.8568366435307,21.2980122757972,-45.2846320174133));
#20648=CARTESIAN_POINT('Ctrl Pts',(-25.7672344770345,21.2108251615749,-45.277158474638));
#20649=CARTESIAN_POINT('Ctrl Pts',(-25.7361440480881,21.1817493376022,-45.2745891283966));
#20650=CARTESIAN_POINT('Ctrl Pts',(-25.6988529112685,21.1482343439667,-45.271531034162));
#20651=CARTESIAN_POINT('Ctrl Pts',(-25.6932000355061,21.1431898072018,-45.271068093199));
#20652=CARTESIAN_POINT('Ctrl Pts',(-25.6850478405084,21.1359663958933,-45.2704013497791));
#20653=CARTESIAN_POINT('Ctrl Pts',(-25.6825628348166,21.1337713446945,-45.270198225376));
#20654=CARTESIAN_POINT('Ctrl Pts',(-25.6776742471662,21.1294665776766,-45.26979885875));
#20655=CARTESIAN_POINT('Ctrl Pts',(-25.6752709029983,21.127356596634,-45.2696026279345));
#20656=CARTESIAN_POINT('Ctrl Pts',(-25.670485784601,21.1231681679802,-45.2692121382054));
#20657=CARTESIAN_POINT('Ctrl Pts',(-25.6681040848658,21.1210896400942,-45.2690178829367));
#20658=CARTESIAN_POINT('Ctrl Pts',(-25.6624694320859,21.116186820468,-45.2685585532779));
#20659=CARTESIAN_POINT('Ctrl Pts',(-25.6592138722089,21.1133655452292,-45.2682933539526));
#20660=CARTESIAN_POINT('Ctrl Pts',(-25.6478538876781,21.1035607724016,-45.2673686161135));
#20661=CARTESIAN_POINT('Ctrl Pts',(-25.6397204216473,21.0966111671023,-45.2667076779282));
#20662=CARTESIAN_POINT('Ctrl Pts',(-25.5389136325498,21.0113419583673,-45.2585296908099));
#20663=CARTESIAN_POINT('Ctrl Pts',(-25.4419348617774,20.9382855523003,-45.2507990142347));
#20664=CARTESIAN_POINT('Ctrl Pts',(-25.2307021859127,20.7971030656318,-45.2342103919956));
#20665=CARTESIAN_POINT('Ctrl Pts',(-25.1158819005871,20.7302273458819,-45.2253295179925));
#20666=CARTESIAN_POINT('Ctrl Pts',(-24.8981456314014,20.6208140689927,-45.2088743000523));
#20667=CARTESIAN_POINT('Ctrl Pts',(-24.7965100460048,20.5761530071109,-45.2013374879993));
#20668=CARTESIAN_POINT('Ctrl Pts',(-24.6144293087517,20.507118381267,-45.1882488061272));
#20669=CARTESIAN_POINT('Ctrl Pts',(-24.5349512615989,20.4804792651584,-45.182668313399));
#20670=CARTESIAN_POINT('Ctrl Pts',(-24.4146005061842,20.445296825031,-45.1744957101365));
#20671=CARTESIAN_POINT('Ctrl Pts',(-24.3744560912716,20.4344001245433,-45.171814989321));
#20672=CARTESIAN_POINT('Ctrl Pts',(-24.3139391802099,20.4192251113258,-45.1678527717216));
#20673=CARTESIAN_POINT('Ctrl Pts',(-24.2937193084048,20.4143623533056,-45.1665420095325));
#20674=CARTESIAN_POINT('Ctrl Pts',(-24.2694769449185,20.4087798747163,-45.1649872770877));
#20675=CARTESIAN_POINT('Ctrl Pts',(-24.2654989748122,20.4078717881873,-45.1647326975547));
#20676=CARTESIAN_POINT('Ctrl Pts',(-24.259350457191,20.406480491751,-45.1643400528222));
#20677=CARTESIAN_POINT('Ctrl Pts',(-24.2571811344344,20.4059919735069,-45.164201681918));
#20678=CARTESIAN_POINT('Ctrl Pts',(-24.2533728059519,20.405138501659,-45.1639590532566));
#20679=CARTESIAN_POINT('Ctrl Pts',(-24.251734027114,20.4047725852287,-45.1638547398956));
#20680=CARTESIAN_POINT('Ctrl Pts',(-24.2479857761102,20.403938728063,-45.1636163653293));
#20681=CARTESIAN_POINT('Ctrl Pts',(-24.2458761228079,20.4034716287975,-45.1634823534853));
#20682=CARTESIAN_POINT('Ctrl Pts',(-24.2401575380812,20.4022115062517,-45.1631195045512));
#20683=CARTESIAN_POINT('Ctrl Pts',(-24.2365476959867,20.4014225643095,-45.1628909033215));
#20684=CARTESIAN_POINT('Ctrl Pts',(-24.219585424991,20.3977459629985,-45.1618187911798));
#20685=CARTESIAN_POINT('Ctrl Pts',(-24.2062158208505,20.3949369584659,-45.1609797517779));
#20686=CARTESIAN_POINT('Ctrl Pts',(-24.1917101658824,20.3919854485543,-45.160075507181));
#20687=CARTESIAN_POINT('Ctrl Pts',(-24.1905917293686,20.3917584954748,-45.1600058259435));
#20688=CARTESIAN_POINT('Ctrl Pts',(-24.1881021061363,20.3912546779936,-45.1598508032302));
#20689=CARTESIAN_POINT('Ctrl Pts',(-24.1867308582596,20.3909781119691,-45.1597654775152));
#20690=CARTESIAN_POINT('Ctrl Pts',(-23.8979647845241,20.3329327196181,-45.1418092839725));
#20691=CARTESIAN_POINT('Ctrl Pts',(-23.6039780835636,20.3146337129784,-45.12599133174));
#20692=CARTESIAN_POINT('Ctrl Pts',(-23.1965119478916,20.3448996337368,-45.1029867512282));
#20693=CARTESIAN_POINT('Ctrl Pts',(-23.0820432226493,20.3596105028491,-45.09641683267));
#20694=CARTESIAN_POINT('Ctrl Pts',(-22.9087625693298,20.3914060299975,-45.086116877009));
#20695=CARTESIAN_POINT('Ctrl Pts',(-22.8492354849055,20.4040810502791,-45.0825141454747));
#20696=CARTESIAN_POINT('Ctrl Pts',(-22.7692935234882,20.4234843524806,-45.0775715287664));
#20697=CARTESIAN_POINT('Ctrl Pts',(-22.7485327837924,20.4287430200786,-45.0762783570718));
#20698=CARTESIAN_POINT('Ctrl Pts',(-22.718304718016,20.4367211964937,-45.0743808356975));
#20699=CARTESIAN_POINT('Ctrl Pts',(-22.7087947158741,20.4392778804321,-45.0737817348839));
#20700=CARTESIAN_POINT('Ctrl Pts',(-22.6917731054205,20.4439377563845,-45.0727055492494));
#20701=CARTESIAN_POINT('Ctrl Pts',(-22.6842571034399,20.4460247170519,-45.0722289936075));
#20702=CARTESIAN_POINT('Ctrl Pts',(-22.6728177865572,20.4492458389132,-45.0715015807294));
#20703=CARTESIAN_POINT('Ctrl Pts',(-22.6688888911746,20.4503602152463,-45.0712513690741));
#20704=CARTESIAN_POINT('Ctrl Pts',(-22.6617898821309,20.4523883372215,-45.0707985814163));
#20705=CARTESIAN_POINT('Ctrl Pts',(-22.6586190283564,20.4532994899673,-45.0705960903513));
#20706=CARTESIAN_POINT('Ctrl Pts',(-22.6518121759099,20.45526677639,-45.0701608681467));
#20707=CARTESIAN_POINT('Ctrl Pts',(-22.648176631097,20.4563244511137,-45.0699280868675));
#20708=CARTESIAN_POINT('Ctrl Pts',(-22.6384190335322,20.4591818510478,-45.0693024272133));
#20709=CARTESIAN_POINT('Ctrl Pts',(-22.632300471429,20.4609933494242,-45.0689091638688));
#20710=CARTESIAN_POINT('Ctrl Pts',(-22.6056200170591,20.4689787878761,-45.0671901720207));
#20711=CARTESIAN_POINT('Ctrl Pts',(-22.585115107875,20.4753398192319,-45.0658583187525));
#20712=CARTESIAN_POINT('Ctrl Pts',(-22.552268549486,20.4858903871596,-45.0637071298217));
#20713=CARTESIAN_POINT('Ctrl Pts',(-22.5398858600029,20.4899508207054,-45.0628920895583));
#20714=CARTESIAN_POINT('Ctrl Pts',(-22.5219253408943,20.4959611802209,-45.0617039196904));
#20715=CARTESIAN_POINT('Ctrl Pts',(-22.5163275962682,20.497851558988,-45.0613327544074));
#20716=CARTESIAN_POINT('Ctrl Pts',(-22.503974508117,20.5020611214996,-45.060511783333));
#20717=CARTESIAN_POINT('Ctrl Pts',(-22.4972216262323,20.5043873858569,-45.0600617471255));
#20718=CARTESIAN_POINT('Ctrl Pts',(-22.4839316283652,20.5090150658228,-45.0591735824255));
#20719=CARTESIAN_POINT('Ctrl Pts',(-22.4773940898212,20.5113151589937,-45.0587354991087));
#20720=CARTESIAN_POINT('Ctrl Pts',(-22.4652019844564,20.5156489361261,-45.0579162832414));
#20721=CARTESIAN_POINT('Ctrl Pts',(-22.4595455780171,20.5176773862581,-45.0575353221834));
#20722=CARTESIAN_POINT('Ctrl Pts',(-22.4500721710333,20.521104588394,-45.0568957809913));
#20723=CARTESIAN_POINT('Ctrl Pts',(-22.4462520679164,20.5224947698972,-45.0566374783523));
#20724=CARTESIAN_POINT('Ctrl Pts',(-22.4292181472484,20.528730141824,-45.0554838642378));
#20725=CARTESIAN_POINT('Ctrl Pts',(-22.4160336771917,20.5336545764127,-45.0545860128434));
#20726=CARTESIAN_POINT('Ctrl Pts',(-22.2398166444256,20.6007906733022,-45.042519248083));
#20727=CARTESIAN_POINT('Ctrl Pts',(-22.0820887129767,20.6760487840267,-45.0309291086369));
#20728=CARTESIAN_POINT('Ctrl Pts',(-21.8293093166297,20.8229148899508,-45.011207636818));
#20729=CARTESIAN_POINT('Ctrl Pts',(-21.7307001781605,20.887688829786,-45.0031940605351));
#20730=CARTESIAN_POINT('Ctrl Pts',(-21.5586145166671,21.0147611735799,-44.9888114403302));
#20731=CARTESIAN_POINT('Ctrl Pts',(-21.4839489874093,21.0752311321703,-44.9824211301116));
#20732=CARTESIAN_POINT('Ctrl Pts',(-21.386717035229,21.1614491172433,-44.9740021201736));
#20733=CARTESIAN_POINT('Ctrl Pts',(-21.3616990588191,21.1843485812641,-44.9718267292021));
#20734=CARTESIAN_POINT('Ctrl Pts',(-21.3240241870501,21.2199422853436,-44.9685428527679));
#20735=CARTESIAN_POINT('Ctrl Pts',(-21.3111047078489,21.2323535811299,-44.9674152789667));
#20736=CARTESIAN_POINT('Ctrl Pts',(-21.2954996388782,21.2475970733138,-44.9660522747915));
#20737=CARTESIAN_POINT('Ctrl Pts',(-21.2927151636425,21.2503269242224,-44.9658090277211));
#20738=CARTESIAN_POINT('Ctrl Pts',(-21.2883787446777,21.2545937363338,-44.9654301518959));
#20739=CARTESIAN_POINT('Ctrl Pts',(-21.2868234091344,21.2561272211838,-44.9652942503991));
#20740=CARTESIAN_POINT('Ctrl Pts',(-21.2840764647279,21.2588410869277,-44.965054211899));
#20741=CARTESIAN_POINT('Ctrl Pts',(-21.2828842245792,21.2600208107505,-44.9649500238509));
#20742=CARTESIAN_POINT('Ctrl Pts',(-21.2803383456023,21.262543899199,-44.9647275312949));
#20743=CARTESIAN_POINT('Ctrl Pts',(-21.2789849819542,21.2638875308775,-44.9646092489906));
#20744=CARTESIAN_POINT('Ctrl Pts',(-21.2750777284315,21.2677735803586,-44.964267735299));
#20745=CARTESIAN_POINT('Ctrl Pts',(-21.2725268987723,21.2703190918492,-44.964044749505));
#20746=CARTESIAN_POINT('Ctrl Pts',(-21.2612154229078,21.2816449148349,-44.963055769378));
#20747=CARTESIAN_POINT('Ctrl Pts',(-21.2525010858741,21.2904716330932,-44.9622934198514));
#20748=CARTESIAN_POINT('Ctrl Pts',(-21.2418492262579,21.3013861844153,-44.9613606875415));
#20749=CARTESIAN_POINT('Ctrl Pts',(-21.2398633854212,21.3034264010395,-44.9611867588706));
#20750=CARTESIAN_POINT('Ctrl Pts',(-21.0631292209979,21.4854819200006,-44.945703906993));
#20751=CARTESIAN_POINT('Ctrl Pts',(-20.9099639989115,21.6853179177608,-44.9319210444006));
#20752=CARTESIAN_POINT('Ctrl Pts',(-20.6991602642798,22.0391963654348,-44.9088777128871));
#20753=CARTESIAN_POINT('Ctrl Pts',(-20.6272754008357,22.1834255272332,-44.8998099401317));
#20754=CARTESIAN_POINT('Ctrl Pts',(-20.5440571046845,22.3873150978992,-44.8869226753958));
#20755=CARTESIAN_POINT('Ctrl Pts',(-20.5231680039762,22.4428262230988,-44.8834091944686));
#20756=CARTESIAN_POINT('Ctrl Pts',(-20.496969542046,22.5187381681002,-44.8785826031711));
#20757=CARTESIAN_POINT('Ctrl Pts',(-20.4903104819024,22.5386629324985,-44.8773137846334));
#20758=CARTESIAN_POINT('Ctrl Pts',(-20.480859788145,22.5678880407044,-44.8754492659968));
#20759=CARTESIAN_POINT('Ctrl Pts',(-20.4779145387035,22.5771384269165,-44.8748586036238));
#20760=CARTESIAN_POINT('Ctrl Pts',(-20.4727015074216,22.5937710139456,-44.8737956069141));
#20761=CARTESIAN_POINT('Ctrl Pts',(-20.4704183708487,22.6011483536146,-44.8733237794919));
#20762=CARTESIAN_POINT('Ctrl Pts',(-20.4669754016512,22.6124166260711,-44.87260256269));
#20763=CARTESIAN_POINT('Ctrl Pts',(-20.46579635802,22.6163016984241,-44.8723538040856));
#20764=CARTESIAN_POINT('Ctrl Pts',(-20.4636692427214,22.6233587282291,-44.8719017659872));
#20765=CARTESIAN_POINT('Ctrl Pts',(-20.4627187097627,22.626529942945,-44.8716985674912));
#20766=CARTESIAN_POINT('Ctrl Pts',(-20.4608245385674,22.6328849582267,-44.8712912289732));
#20767=CARTESIAN_POINT('Ctrl Pts',(-20.4598809313744,22.6360687638598,-44.8710870882142));
#20768=CARTESIAN_POINT('Ctrl Pts',(-20.4572604662097,22.6449608429802,-44.8705167492959));
#20769=CARTESIAN_POINT('Ctrl Pts',(-20.4555944982706,22.6506722883516,-44.8701501954468));
#20770=CARTESIAN_POINT('Ctrl Pts',(-20.4489552411344,22.6736703958866,-44.8686732901961));
#20771=CARTESIAN_POINT('Ctrl Pts',(-20.4441109798194,22.6909936860314,-44.8675587366589));
#20772=CARTESIAN_POINT('Ctrl Pts',(-20.4352859533609,22.7236025156855,-44.8654565659501));
#20773=CARTESIAN_POINT('Ctrl Pts',(-20.4312720338651,22.7388785902106,-44.8644700665219));
#20774=CARTESIAN_POINT('Ctrl Pts',(-20.4260742069639,22.7592690282358,-44.8631509158559));
#20775=CARTESIAN_POINT('Ctrl Pts',(-20.4247902197799,22.7643578544405,-44.8628215000721));
#20776=CARTESIAN_POINT('Ctrl Pts',(-20.4226914948034,22.7727622233332,-44.8622771308827));
#20777=CARTESIAN_POINT('Ctrl Pts',(-20.4218695814428,22.7760759785073,-44.8620624077709));
#20778=CARTESIAN_POINT('Ctrl Pts',(-20.4206782507937,22.7809120111051,-44.8617489214697));
#20779=CARTESIAN_POINT('Ctrl Pts',(-20.4203046731385,22.782433269756,-44.8616502910719));
#20780=CARTESIAN_POINT('Ctrl Pts',(-20.4189846294926,22.787825637859,-44.8613006150651));
#20781=CARTESIAN_POINT('Ctrl Pts',(-20.4180442377539,22.7916982179214,-44.861049376423));
#20782=CARTESIAN_POINT('Ctrl Pts',(-20.4154813042982,22.802338533051,-44.8603587527368));
#20783=CARTESIAN_POINT('Ctrl Pts',(-20.4138735052767,22.8091097661576,-44.8599189022605));
#20784=CARTESIAN_POINT('Ctrl Pts',(-20.4093289806717,22.8285286259707,-44.8586564514283));
#20785=CARTESIAN_POINT('Ctrl Pts',(-20.4064467644044,22.8411887551764,-44.8578321493275));
#20786=CARTESIAN_POINT('Ctrl Pts',(-20.4010661933736,22.8655007723999,-44.8562467672213));
#20787=CARTESIAN_POINT('Ctrl Pts',(-20.3985558021515,22.8771498022945,-44.8554860727357));
#20788=CARTESIAN_POINT('Ctrl Pts',(-20.3270481729637,23.2181409589842,-44.8331876894662));
#20789=CARTESIAN_POINT('Ctrl Pts',(-20.3100026497799,23.5562321470106,-44.8099080844745));
#20790=CARTESIAN_POINT('Ctrl Pts',(-20.3532325366874,23.9631548564351,-44.7827384640491));
#20791=CARTESIAN_POINT('Ctrl Pts',(-20.3633838722017,24.0353246763728,-44.7779665758087));
#20792=CARTESIAN_POINT('Ctrl Pts',(-20.3811660052329,24.1366919355419,-44.7713851975304));
#20793=CARTESIAN_POINT('Ctrl Pts',(-20.3867722033162,24.1662175951536,-44.76948292917));
#20794=CARTESIAN_POINT('Ctrl Pts',(-20.3936936770142,24.2000787267925,-44.7673216673449));
#20795=CARTESIAN_POINT('Ctrl Pts',(-20.3946058044604,24.2044937871827,-44.7670402654172));
#20796=CARTESIAN_POINT('Ctrl Pts',(-20.3960002440421,24.2111726672493,-44.7666151942605));
#20797=CARTESIAN_POINT('Ctrl Pts',(-20.39647573059,24.2134378818333,-44.7664711347015));
#20798=CARTESIAN_POINT('Ctrl Pts',(-20.3973390118192,24.2175286226634,-44.7662111756556));
#20799=CARTESIAN_POINT('Ctrl Pts',(-20.3977259508137,24.2193543193829,-44.7660952272359));
#20800=CARTESIAN_POINT('Ctrl Pts',(-20.3985049166878,24.2230140429887,-44.7658629444919));
#20801=CARTESIAN_POINT('Ctrl Pts',(-20.3988969570447,24.2248480563953,-44.7657466114873));
#20802=CARTESIAN_POINT('Ctrl Pts',(-20.4000140301585,24.2300516384619,-44.7654167452201));
#20803=CARTESIAN_POINT('Ctrl Pts',(-20.4007428706314,24.2334204007105,-44.765203431752));
#20804=CARTESIAN_POINT('Ctrl Pts',(-20.4038348006572,24.2476014497764,-44.7643064578189));
#20805=CARTESIAN_POINT('Ctrl Pts',(-20.4062482108974,24.258402862455,-44.7636256628503));
#20806=CARTESIAN_POINT('Ctrl Pts',(-20.4500295747269,24.4497134534795,-44.751607025997));
#20807=CARTESIAN_POINT('Ctrl Pts',(-20.5068321490864,24.6263689912586,-44.741121579045));
#20808=CARTESIAN_POINT('Ctrl Pts',(-20.6480721669903,24.9629775227874,-44.7206642480205));
#20809=CARTESIAN_POINT('Ctrl Pts',(-20.7313850065157,25.1226475079508,-44.7107148208347));
#20810=CARTESIAN_POINT('Ctrl Pts',(-20.8966685795722,25.3836335752822,-44.6929930723686));
#20811=CARTESIAN_POINT('Ctrl Pts',(-20.9722480863356,25.4884684021089,-44.6854184352356));
#20812=CARTESIAN_POINT('Ctrl Pts',(-21.0607872971317,25.5969080500766,-44.6769300379716));
#20813=CARTESIAN_POINT('Ctrl Pts',(-21.067711742607,25.6053017259999,-44.6762685646686));
#20814=CARTESIAN_POINT('Ctrl Pts',(-21.0801029305507,25.6201680586037,-44.6750889957753));
#20815=CARTESIAN_POINT('Ctrl Pts',(-21.0855529633116,25.6266545582839,-44.6745715827647));
#20816=CARTESIAN_POINT('Ctrl Pts',(-21.093756083571,25.6363399158125,-44.6737948512717));
#20817=CARTESIAN_POINT('Ctrl Pts',(-21.0964900108697,25.6395550145692,-44.6735363215207));
#20818=CARTESIAN_POINT('Ctrl Pts',(-21.1013369479442,25.6452323773558,-44.6730785711106));
#20819=CARTESIAN_POINT('Ctrl Pts',(-21.1034473797392,25.6476968428271,-44.6728794571511));
#20820=CARTESIAN_POINT('Ctrl Pts',(-21.1076658383732,25.6526079340681,-44.672481847716));
#20821=CARTESIAN_POINT('Ctrl Pts',(-21.1097738284339,25.6550545867801,-44.6722833538897));
#20822=CARTESIAN_POINT('Ctrl Pts',(-21.1154770028903,25.6616539281768,-44.6717468486042));
#20823=CARTESIAN_POINT('Ctrl Pts',(-21.1190791200695,25.6658005871027,-44.6714085490555));
#20824=CARTESIAN_POINT('Ctrl Pts',(-21.1324312436267,25.6810920496013,-44.670156591904));
#20825=CARTESIAN_POINT('Ctrl Pts',(-21.1422473104427,25.6921786916639,-44.6692401757693));
#20826=CARTESIAN_POINT('Ctrl Pts',(-21.3122523665041,25.8815432351422,-44.6534351708116));
#20827=CARTESIAN_POINT('Ctrl Pts',(-21.4917252325096,26.0414332269614,-44.6376683242449));
#20828=CARTESIAN_POINT('Ctrl Pts',(-21.7030871302608,26.1911758316436,-44.6201957948438));
#20829=CARTESIAN_POINT('Ctrl Pts',(-21.7190598699247,26.2022761598967,-44.6188820847764));
#20830=CARTESIAN_POINT('Ctrl Pts',(-21.8441975835271,26.2875716355257,-44.6086448226165));
#20831=CARTESIAN_POINT('Ctrl Pts',(-21.9577136023082,26.3551323111444,-44.5996747431003));
#20832=CARTESIAN_POINT('Ctrl Pts',(-22.0750360439056,26.4155367892604,-44.590879968079));
#20833=CARTESIAN_POINT('Origin',(-23.5502525316942,23.5502525316942,-77.3107734492734));
#20834=CARTESIAN_POINT('',(-22.0750360145756,26.4155367741596,-43.0932330566435));
#20835=CARTESIAN_POINT('',(-22.0750361136176,26.4155368251522,-43.341564988124));
#20836=CARTESIAN_POINT('',(-22.0750360153461,26.4155367745563,-77.3107734492734));
#20837=CARTESIAN_POINT('',(-26.7730011356003,23.5532335332771,-43.9391856912327));
#20838=CARTESIAN_POINT('Ctrl Pts',(-22.0750360145756,26.4155367741596,-43.0932330566435));
#20839=CARTESIAN_POINT('Ctrl Pts',(-22.0509411675559,26.4031313325723,-43.0949199058338));
#20840=CARTESIAN_POINT('Ctrl Pts',(-22.0270038178035,26.3904224862259,-43.09661747516));
#20841=CARTESIAN_POINT('Ctrl Pts',(-21.930883109556,26.337825215561,-43.103524041299));
#20842=CARTESIAN_POINT('Ctrl Pts',(-21.8600885552139,26.2954779462133,-43.1088193988789));
#20843=CARTESIAN_POINT('Ctrl Pts',(-21.5833383513035,26.1151687011008,-43.1303745886662));
#20844=CARTESIAN_POINT('Ctrl Pts',(-21.3919924743565,25.9563764069618,-43.1473357358126));
#20845=CARTESIAN_POINT('Ctrl Pts',(-21.1258009127753,25.6779357062376,-43.1732132722146));
#20846=CARTESIAN_POINT('Ctrl Pts',(-21.0372778885744,25.5726199210681,-43.1823014093251));
#20847=CARTESIAN_POINT('Ctrl Pts',(-20.950887762283,25.4553738640371,-43.1914490342169));
#20848=CARTESIAN_POINT('Ctrl Pts',(-20.9460597476488,25.4487689109754,-43.1919612533885));
#20849=CARTESIAN_POINT('Ctrl Pts',(-20.9394677329414,25.4396782607697,-43.192661909344));
#20850=CARTESIAN_POINT('Ctrl Pts',(-20.9376820826013,25.4372084134788,-43.1928518345535));
#20851=CARTESIAN_POINT('Ctrl Pts',(-20.9348500783737,25.4332795610114,-43.1931532555518));
#20852=CARTESIAN_POINT('Ctrl Pts',(-20.9338014411278,25.4318222159437,-43.1932649105526));
#20853=CARTESIAN_POINT('Ctrl Pts',(-20.9317630011989,25.4289842919179,-43.1934820416224));
#20854=CARTESIAN_POINT('Ctrl Pts',(-20.9307730750831,25.4276038106479,-43.1935875260526));
#20855=CARTESIAN_POINT('Ctrl Pts',(-20.9283896780335,25.4242745376001,-43.193841591688));
#20856=CARTESIAN_POINT('Ctrl Pts',(-20.9269972849552,25.4223249695479,-43.1939900974984));
#20857=CARTESIAN_POINT('Ctrl Pts',(-20.9228169131104,25.4164579736698,-43.1944362003183));
#20858=CARTESIAN_POINT('Ctrl Pts',(-20.9200355100866,25.4125358349052,-43.1947333425803));
#20859=CARTESIAN_POINT('Ctrl Pts',(-20.8966778283354,25.3794417613896,-43.1972315970212));
#20860=CARTESIAN_POINT('Ctrl Pts',(-20.8765777541089,25.3499345558076,-43.1994005413393));
#20861=CARTESIAN_POINT('Ctrl Pts',(-20.8033881603989,25.2385575013189,-43.2073957699233));
#20862=CARTESIAN_POINT('Ctrl Pts',(-20.7535308021796,25.1546180052873,-43.2130428969139));
#20863=CARTESIAN_POINT('Ctrl Pts',(-20.61283514177,24.8911925405185,-43.2300363220955));
#20864=CARTESIAN_POINT('Ctrl Pts',(-20.5349167902404,24.7053699118333,-43.241063335693));
#20865=CARTESIAN_POINT('Ctrl Pts',(-20.4226323126586,24.3468683586313,-43.2623523678401));
#20866=CARTESIAN_POINT('Ctrl Pts',(-20.3840793568824,24.1763027509273,-43.2724862112721));
#20867=CARTESIAN_POINT('Ctrl Pts',(-20.3579134738227,23.9920907363947,-43.2838008872555));
#20868=CARTESIAN_POINT('Ctrl Pts',(-20.3563580576937,23.9807031597127,-43.2845017201422));
#20869=CARTESIAN_POINT('Ctrl Pts',(-20.354285982917,23.9649031253491,-43.2854761062605));
#20870=CARTESIAN_POINT('Ctrl Pts',(-20.3537174708215,23.9604974585504,-43.2857480178683));
#20871=CARTESIAN_POINT('Ctrl Pts',(-20.3527555823451,23.9529199339334,-43.2862160662392));
#20872=CARTESIAN_POINT('Ctrl Pts',(-20.3523578111157,23.9497486316861,-43.2864120637698));
#20873=CARTESIAN_POINT('Ctrl Pts',(-20.3515480318244,23.9432138122725,-43.2868161725079));
#20874=CARTESIAN_POINT('Ctrl Pts',(-20.3511366100199,23.9398502281367,-43.2870243019567));
#20875=CARTESIAN_POINT('Ctrl Pts',(-20.350193734576,23.9320395361099,-43.2875079056571));
#20876=CARTESIAN_POINT('Ctrl Pts',(-20.3496662457684,23.927591964797,-43.2877835048707));
#20877=CARTESIAN_POINT('Ctrl Pts',(-20.3480544367186,23.9137552885425,-43.2886416200268));
#20878=CARTESIAN_POINT('Ctrl Pts',(-20.3470021553277,23.9043625667906,-43.2892251469476));
#20879=CARTESIAN_POINT('Ctrl Pts',(-20.337285020128,23.8140374283075,-43.2948466070312));
#20880=CARTESIAN_POINT('Ctrl Pts',(-20.3316485479049,23.732815267769,-43.2999795957716));
#20881=CARTESIAN_POINT('Ctrl Pts',(-20.3281365440153,23.6210513809252,-43.3071594480434));
#20882=CARTESIAN_POINT('Ctrl Pts',(-20.3276116339609,23.5906191540321,-43.3091261755423));
#20883=CARTESIAN_POINT('Ctrl Pts',(-20.3268423603734,23.3410125783794,-43.3253524121541));
#20884=CARTESIAN_POINT('Ctrl Pts',(-20.348527276048,23.1223654367842,-43.3402244465518));
#20885=CARTESIAN_POINT('Ctrl Pts',(-20.4223257031285,22.7596908600062,-43.3652397117691));
#20886=CARTESIAN_POINT('Ctrl Pts',(-20.4627952842113,22.6140199553117,-43.3753689358388));
#20887=CARTESIAN_POINT('Ctrl Pts',(-20.514100827385,22.4695557091456,-43.3851768718604));
#20888=CARTESIAN_POINT('Ctrl Pts',(-20.5148685743261,22.4674011913597,-43.385323089076));
#20889=CARTESIAN_POINT('Ctrl Pts',(-20.5250485645522,22.438929121007,-43.3872545889702));
#20890=CARTESIAN_POINT('Ctrl Pts',(-20.5348008887788,22.4127331758003,-43.3890230008916));
#20891=CARTESIAN_POINT('Ctrl Pts',(-20.5466000703984,22.3822577527964,-43.391067360424));
#20892=CARTESIAN_POINT('Ctrl Pts',(-20.5483166647578,22.3778528714839,-43.3913625312122));
#20893=CARTESIAN_POINT('Ctrl Pts',(-20.5509164751562,22.3712247521225,-43.3918061835212));
#20894=CARTESIAN_POINT('Ctrl Pts',(-20.5517924744881,22.3689987187988,-43.3919550981166));
#20895=CARTESIAN_POINT('Ctrl Pts',(-20.5533588347952,22.3650313536954,-43.3922203486137));
#20896=CARTESIAN_POINT('Ctrl Pts',(-20.5540482347313,22.363289650127,-43.3923367426168));
#20897=CARTESIAN_POINT('Ctrl Pts',(-20.5555149565223,22.3595935367529,-43.3925836320781));
#20898=CARTESIAN_POINT('Ctrl Pts',(-20.5562926711997,22.3576392917081,-43.3927141029301));
#20899=CARTESIAN_POINT('Ctrl Pts',(-20.5578820544281,22.3536568348538,-43.3929798490574));
#20900=CARTESIAN_POINT('Ctrl Pts',(-20.5586938733969,22.3516286837144,-43.3931151151122));
#20901=CARTESIAN_POINT('Ctrl Pts',(-20.5622993115452,22.3426477694502,-43.3937137833543));
#20902=CARTESIAN_POINT('Ctrl Pts',(-20.5651151416482,22.3357038612845,-43.3941758483552));
#20903=CARTESIAN_POINT('Ctrl Pts',(-20.5920069388273,22.2700465007535,-43.3985376866179));
#20904=CARTESIAN_POINT('Ctrl Pts',(-20.6177898714931,22.2120415877526,-43.4023368314478));
#20905=CARTESIAN_POINT('Ctrl Pts',(-20.6729204209858,22.0972710564713,-43.4098170670278));
#20906=CARTESIAN_POINT('Ctrl Pts',(-20.7022759620202,22.0405421107163,-43.4134956255235));
#20907=CARTESIAN_POINT('Ctrl Pts',(-20.8121204999002,21.8428924562843,-43.4263720995039));
#20908=CARTESIAN_POINT('Ctrl Pts',(-20.9015424225747,21.7072159658174,-43.4353327702715));
#20909=CARTESIAN_POINT('Ctrl Pts',(-21.13121880199,21.4101953444886,-43.4564178222973));
#20910=CARTESIAN_POINT('Ctrl Pts',(-21.2780226763631,21.2549268810314,-43.4686259340821));
#20911=CARTESIAN_POINT('Ctrl Pts',(-21.4489751884401,21.1067052865176,-43.4823703505936));
#20912=CARTESIAN_POINT('Ctrl Pts',(-21.4589378525004,21.0981733084019,-43.4831696123388));
#20913=CARTESIAN_POINT('Ctrl Pts',(-21.4725393929948,21.0866682017941,-43.4842585847397));
#20914=CARTESIAN_POINT('Ctrl Pts',(-21.4761331918699,21.0836417798647,-43.4845461042142));
#20915=CARTESIAN_POINT('Ctrl Pts',(-21.4822362324827,21.0785250357067,-43.485034026552));
#20916=CARTESIAN_POINT('Ctrl Pts',(-21.4847420649467,21.0764306424176,-43.4852342625583));
#20917=CARTESIAN_POINT('Ctrl Pts',(-21.4895754972568,21.0724032876278,-43.4856203044036));
#20918=CARTESIAN_POINT('Ctrl Pts',(-21.4919026446797,21.0704697873581,-43.4858060879171));
#20919=CARTESIAN_POINT('Ctrl Pts',(-21.4974014018514,21.0659142424378,-43.4862448759366));
#20920=CARTESIAN_POINT('Ctrl Pts',(-21.5005753122253,21.0632949943601,-43.4864979938534));
#20921=CARTESIAN_POINT('Ctrl Pts',(-21.5071413582922,21.0578975166931,-43.4870213224489));
#20922=CARTESIAN_POINT('Ctrl Pts',(-21.5105341628678,21.0551201177233,-43.4872915661259));
#20923=CARTESIAN_POINT('Ctrl Pts',(-21.5290512781828,21.0400247466253,-43.4887655775794));
#20924=CARTESIAN_POINT('Ctrl Pts',(-21.5442812535625,21.0278375689044,-43.4899746138252));
#20925=CARTESIAN_POINT('Ctrl Pts',(-21.5839344893001,20.9966929053899,-43.4931144886326));
#20926=CARTESIAN_POINT('Ctrl Pts',(-21.608521147046,20.9779476253101,-43.4950536277252));
#20927=CARTESIAN_POINT('Ctrl Pts',(-21.7138836280822,20.8999888790961,-43.5033333371192));
#20928=CARTESIAN_POINT('Ctrl Pts',(-21.7971196442831,20.8442093240221,-43.5098027894704));
#20929=CARTESIAN_POINT('Ctrl Pts',(-22.020984040137,20.7088573407347,-43.5270118794189));
#20930=CARTESIAN_POINT('Ctrl Pts',(-22.1652303784352,20.6358238695582,-43.5379265022705));
#20931=CARTESIAN_POINT('Ctrl Pts',(-22.4957677786971,20.4985683293647,-43.5621518756575));
#20932=CARTESIAN_POINT('Ctrl Pts',(-22.6837406905633,20.4399645917796,-43.5754235621738));
#20933=CARTESIAN_POINT('Ctrl Pts',(-22.8875641391993,20.3963495654122,-43.5885643782032));
#20934=CARTESIAN_POINT('Ctrl Pts',(-22.8992415203174,20.3939185031191,-43.5893129023727));
#20935=CARTESIAN_POINT('Ctrl Pts',(-22.9144110619574,20.3908481914616,-43.5902794170298));
#20936=CARTESIAN_POINT('Ctrl Pts',(-22.9178909598769,20.3901498430943,-43.5905007365136));
#20937=CARTESIAN_POINT('Ctrl Pts',(-22.9232316319113,20.3890872483263,-43.5908397802094));
#20938=CARTESIAN_POINT('Ctrl Pts',(-22.9250915712984,20.3887188957549,-43.5909577400968));
#20939=CARTESIAN_POINT('Ctrl Pts',(-22.9287633078862,20.3879950918075,-43.5911903776596));
#20940=CARTESIAN_POINT('Ctrl Pts',(-22.9305750757971,20.3876395578835,-43.5913050592661));
#20941=CARTESIAN_POINT('Ctrl Pts',(-22.9346162498314,20.3868501403777,-43.5915606130374));
#20942=CARTESIAN_POINT('Ctrl Pts',(-22.9368458042925,20.3864170574972,-43.5917014384353));
#20943=CARTESIAN_POINT('Ctrl Pts',(-22.9414522046534,20.3855273331717,-43.5919920531183));
#20944=CARTESIAN_POINT('Ctrl Pts',(-22.943829111907,20.3850710114029,-43.5921418239974));
#20945=CARTESIAN_POINT('Ctrl Pts',(-22.9565032161387,20.3826526209519,-43.5929394460822));
#20946=CARTESIAN_POINT('Ctrl Pts',(-22.9668095846618,20.3807380927009,-43.5935845986867));
#20947=CARTESIAN_POINT('Ctrl Pts',(-23.0707428243228,20.3619554186031,-43.6000573956181));
#20948=CARTESIAN_POINT('Ctrl Pts',(-23.1650740556054,20.3491887229214,-43.6056617280261));
#20949=CARTESIAN_POINT('Ctrl Pts',(-23.4158465504955,20.3264986019552,-43.6201733701816));
#20950=CARTESIAN_POINT('Ctrl Pts',(-23.5726820099204,20.3237750440163,-43.6288620410276));
#20951=CARTESIAN_POINT('Ctrl Pts',(-23.9731936088545,20.346035988815,-43.6512946120207));
#20952=CARTESIAN_POINT('Ctrl Pts',(-24.2149080607951,20.3873281251913,-43.6651257297402));
#20953=CARTESIAN_POINT('Ctrl Pts',(-24.4641986666611,20.45977511806,-43.6808746572005));
#20954=CARTESIAN_POINT('Ctrl Pts',(-24.4787511637168,20.4641160376623,-43.6817992341494));
#20955=CARTESIAN_POINT('Ctrl Pts',(-24.4985797232819,20.4701837163419,-43.683066344267));
#20956=CARTESIAN_POINT('Ctrl Pts',(-24.5038829705225,20.4718215425147,-43.6834059571441));
#20957=CARTESIAN_POINT('Ctrl Pts',(-24.5122759306501,20.4744373478704,-43.6839445783091));
#20958=CARTESIAN_POINT('Ctrl Pts',(-24.5153684618371,20.4754063068497,-43.6841432897073));
#20959=CARTESIAN_POINT('Ctrl Pts',(-24.5213520814412,20.477291024612,-43.6845282494803));
#20960=CARTESIAN_POINT('Ctrl Pts',(-24.5242433503916,20.4782062031824,-43.6847144785845));
#20961=CARTESIAN_POINT('Ctrl Pts',(-24.5311087193042,20.4803899770237,-43.6851572020395));
#20962=CARTESIAN_POINT('Ctrl Pts',(-24.5350816490168,20.4816622079864,-43.6854138160133));
#20963=CARTESIAN_POINT('Ctrl Pts',(-24.543299760506,20.4843114556736,-43.6859454903174));
#20964=CARTESIAN_POINT('Ctrl Pts',(-24.5475445723407,20.4856895831446,-43.6862205869046));
#20965=CARTESIAN_POINT('Ctrl Pts',(-24.5714508312109,20.4935059573867,-43.6877725995387));
#20966=CARTESIAN_POINT('Ctrl Pts',(-24.5910524237005,20.5001244787869,-43.6890554664467));
#20967=CARTESIAN_POINT('Ctrl Pts',(-24.6420907740677,20.517906959013,-43.6924233899346));
#20968=CARTESIAN_POINT('Ctrl Pts',(-24.6734196569644,20.5293708899276,-43.6945183180815));
#20969=CARTESIAN_POINT('Ctrl Pts',(-24.8123832170093,20.5826812133356,-43.7039371486519));
#20970=CARTESIAN_POINT('Ctrl Pts',(-24.9178895854968,20.629804422128,-43.711434387635));
#20971=CARTESIAN_POINT('Ctrl Pts',(-25.1273611009064,20.7372057591243,-43.7270165065939));
#20972=CARTESIAN_POINT('Ctrl Pts',(-25.2309472919627,20.7978416674148,-43.7351011477651));
#20973=CARTESIAN_POINT('Ctrl Pts',(-25.5127154675556,20.9846266102452,-43.7579778811962));
#20974=CARTESIAN_POINT('Ctrl Pts',(-25.6818387317231,21.1233081791136,-43.7728120429735));
#20975=CARTESIAN_POINT('Ctrl Pts',(-25.8444607642891,21.2868741387223,-43.7873606536753));
#20976=CARTESIAN_POINT('Ctrl Pts',(-25.8532044227488,21.2957712689919,-43.7881437297337));
#20977=CARTESIAN_POINT('Ctrl Pts',(-25.8644127238423,21.3073095520401,-43.7891483607205));
#20978=CARTESIAN_POINT('Ctrl Pts',(-25.8669247363571,21.3099042325787,-43.7893735731497));
#20979=CARTESIAN_POINT('Ctrl Pts',(-25.8707576310827,21.313876604251,-43.7897172826972));
#20980=CARTESIAN_POINT('Ctrl Pts',(-25.8720816491104,21.3152512442902,-43.7898360258242));
#20981=CARTESIAN_POINT('Ctrl Pts',(-25.8745668155211,21.3178360192205,-43.7900589294994));
#20982=CARTESIAN_POINT('Ctrl Pts',(-25.8757282358848,21.319045879584,-43.7901631113578));
#20983=CARTESIAN_POINT('Ctrl Pts',(-25.8783985118063,21.3218318760326,-43.7904026634742));
#20984=CARTESIAN_POINT('Ctrl Pts',(-25.879906708732,21.3234086353311,-43.790537981753));
#20985=CARTESIAN_POINT('Ctrl Pts',(-25.8829983585549,21.3266474095249,-43.7908154083975));
#20986=CARTESIAN_POINT('Ctrl Pts',(-25.8845816398346,21.3283095875483,-43.7909575033429));
#20987=CARTESIAN_POINT('Ctrl Pts',(-25.8885964035542,21.3325334391033,-43.7913178733926));
#20988=CARTESIAN_POINT('Ctrl Pts',(-25.8910254611662,21.335097428854,-43.7915359613267));
#20989=CARTESIAN_POINT('Ctrl Pts',(-25.9246373957772,21.3706935010755,-43.7945545605907));
#20990=CARTESIAN_POINT('Ctrl Pts',(-25.9551246576252,21.4043793695039,-43.7973023613202));
#20991=CARTESIAN_POINT('Ctrl Pts',(-26.0588020540511,21.5239203662249,-43.8067287131811));
#20992=CARTESIAN_POINT('Ctrl Pts',(-26.1281944655074,21.6129702010591,-43.813187838189));
#20993=CARTESIAN_POINT('Ctrl Pts',(-26.2176084750917,21.7410506752079,-43.8220053197226));
#20994=CARTESIAN_POINT('Ctrl Pts',(-26.2417178399554,21.7771158531775,-43.8244393960341));
#20995=CARTESIAN_POINT('Ctrl Pts',(-26.2895124925356,21.8518337850288,-43.8294048548734));
#20996=CARTESIAN_POINT('Ctrl Pts',(-26.313124936592,21.8905213876216,-43.8319351524646));
#20997=CARTESIAN_POINT('Ctrl Pts',(-26.4229062984415,22.0792302191516,-43.8441361506689));
#20998=CARTESIAN_POINT('Ctrl Pts',(-26.497711834573,22.2355194720664,-43.8538380577828));
#20999=CARTESIAN_POINT('Ctrl Pts',(-26.5700302623551,22.4242382821998,-43.8656427933311));
#21000=CARTESIAN_POINT('Ctrl Pts',(-26.5800816549773,22.4515710297423,-43.8673540510259));
#21001=CARTESIAN_POINT('Ctrl Pts',(-26.5931986717294,22.4887897154795,-43.8696883603576));
#21002=CARTESIAN_POINT('Ctrl Pts',(-26.5965893012321,22.4985601791344,-43.8703015302585));
#21003=CARTESIAN_POINT('Ctrl Pts',(-26.6172178335677,22.5589403280299,-43.8740935436191));
#21004=CARTESIAN_POINT('Ctrl Pts',(-26.6332403294934,22.6099537648394,-43.8773092123728));
#21005=CARTESIAN_POINT('Ctrl Pts',(-26.650401775007,22.6697589496453,-43.8811007974053));
#21006=CARTESIAN_POINT('Ctrl Pts',(-26.6527833098899,22.6781877136872,-43.8816356638887));
#21007=CARTESIAN_POINT('Ctrl Pts',(-26.6562809560341,22.6907623209282,-43.8824343815505));
#21008=CARTESIAN_POINT('Ctrl Pts',(-26.6574232042868,22.6949009044045,-43.8826973808729));
#21009=CARTESIAN_POINT('Ctrl Pts',(-26.6594454733324,22.7022854774641,-43.8831668816874));
#21010=CARTESIAN_POINT('Ctrl Pts',(-26.6603286910237,22.7055305913927,-43.8833732788157));
#21011=CARTESIAN_POINT('Ctrl Pts',(-26.6621797728984,22.7123740840218,-43.8838087070617));
#21012=CARTESIAN_POINT('Ctrl Pts',(-26.6631464785182,22.7159727685076,-43.8840377754976));
#21013=CARTESIAN_POINT('Ctrl Pts',(-26.6650967834387,22.7232836099785,-43.8845033340359));
#21014=CARTESIAN_POINT('Ctrl Pts',(-26.666079993025,22.726995863867,-43.8847398363881));
#21015=CARTESIAN_POINT('Ctrl Pts',(-26.6684967646987,22.7361870919654,-43.8853256574845));
#21016=CARTESIAN_POINT('Ctrl Pts',(-26.6699225198927,22.7416680890393,-43.8856752291155));
#21017=CARTESIAN_POINT('Ctrl Pts',(-26.6738405014706,22.7568945152182,-43.8866470035722));
#21018=CARTESIAN_POINT('Ctrl Pts',(-26.6763015432764,22.7666478349685,-43.8872702148627));
#21019=CARTESIAN_POINT('Ctrl Pts',(-26.7415982445304,23.0306279515672,-43.9041585040978));
#21020=CARTESIAN_POINT('Ctrl Pts',(-26.7732432702996,23.2914917503899,-43.9214885813748));
#21021=CARTESIAN_POINT('Ctrl Pts',(-26.7730011528923,23.5532336498954,-43.9391856718898));
#21022=CARTESIAN_POINT('Ctrl Pts',(-26.7730011529985,23.5532335351257,-43.9391856641299));
#21023=CARTESIAN_POINT('Ctrl Pts',(-26.7728064224409,23.7637558140599,-43.9534196550246));
#21024=CARTESIAN_POINT('Ctrl Pts',(-26.7519842051116,23.9737757280023,-43.9677792446346));
#21025=CARTESIAN_POINT('Ctrl Pts',(-26.7047525355364,24.2107145975974,-43.9832586569748));
#21026=CARTESIAN_POINT('Ctrl Pts',(-26.698246890775,24.2410579347819,-43.9852263806559));
#21027=CARTESIAN_POINT('Ctrl Pts',(-26.6904240561525,24.2751358443274,-43.9874161333868));
#21028=CARTESIAN_POINT('Ctrl Pts',(-26.68953739194,24.2789661836675,-43.9876619722946));
#21029=CARTESIAN_POINT('Ctrl Pts',(-26.6880837960387,24.2851937449196,-43.9880611900244));
#21030=CARTESIAN_POINT('Ctrl Pts',(-26.6875211247066,24.2875919418643,-43.9882148105837));
#21031=CARTESIAN_POINT('Ctrl Pts',(-26.6864272837871,24.2922301503398,-43.9885116915697));
#21032=CARTESIAN_POINT('Ctrl Pts',(-26.6858964628286,24.2944702414108,-43.9886549719671));
#21033=CARTESIAN_POINT('Ctrl Pts',(-26.6849311846578,24.2985243971933,-43.9889140950309));
#21034=CARTESIAN_POINT('Ctrl Pts',(-26.6844975540301,24.3003386481243,-43.9890299851679));
#21035=CARTESIAN_POINT('Ctrl Pts',(-26.6835573191463,24.3042574103085,-43.9892801584192));
#21036=CARTESIAN_POINT('Ctrl Pts',(-26.6830501711172,24.3063617820915,-43.9894144091693));
#21037=CARTESIAN_POINT('Ctrl Pts',(-26.6816675884769,24.3120734315302,-43.9897785441984));
#21038=CARTESIAN_POINT('Ctrl Pts',(-26.6807880377044,24.31567972432,-43.9900081897754));
#21039=CARTESIAN_POINT('Ctrl Pts',(-26.676602161561,24.3327145505152,-43.9910917272369));
#21040=CARTESIAN_POINT('Ctrl Pts',(-26.6732155873367,24.3461234938437,-43.9919410316794));
#21041=CARTESIAN_POINT('Ctrl Pts',(-26.6125353569683,24.5800308387846,-44.0067000471658));
#21042=CARTESIAN_POINT('Ctrl Pts',(-26.532095525908,24.793903359641,-44.0193446485638));
#21043=CARTESIAN_POINT('Ctrl Pts',(-26.4095802799876,25.037659597885,-44.0345883897453));
#21044=CARTESIAN_POINT('Ctrl Pts',(-26.3885729915567,25.077364798808,-44.0370985389698));
#21045=CARTESIAN_POINT('Ctrl Pts',(-26.3452575063813,25.1552506237087,-44.0420962992416));
#21046=CARTESIAN_POINT('Ctrl Pts',(-26.322979885118,25.1934368176919,-44.0445830912485));
#21047=CARTESIAN_POINT('Ctrl Pts',(-26.2341824592457,25.3386946082248,-44.0542170830922));
#21048=CARTESIAN_POINT('Ctrl Pts',(-26.1621944183185,25.4422778503158,-44.0614652258796));
#21049=CARTESIAN_POINT('Ctrl Pts',(-26.0499242335088,25.5851629186638,-44.0722407816024));
#21050=CARTESIAN_POINT('Ctrl Pts',(-26.0143898338377,25.628050808158,-44.0755842125731));
#21051=CARTESIAN_POINT('Ctrl Pts',(-25.9730248206347,25.6754216798197,-44.0794118503892));
#21052=CARTESIAN_POINT('Ctrl Pts',(-25.9682677311354,25.6808327264182,-44.0798511089894));
#21053=CARTESIAN_POINT('Ctrl Pts',(-25.9605173452598,25.689589167691,-44.080565279666));
#21054=CARTESIAN_POINT('Ctrl Pts',(-25.9575351157197,25.6929443606694,-44.0808397284495));
#21055=CARTESIAN_POINT('Ctrl Pts',(-25.9517554211544,25.6994195784357,-44.0813709473472));
#21056=CARTESIAN_POINT('Ctrl Pts',(-25.9489588602203,25.7025404009419,-44.0816276791472));
#21057=CARTESIAN_POINT('Ctrl Pts',(-25.9441262661089,25.7079122172302,-44.0820708061248));
#21058=CARTESIAN_POINT('Ctrl Pts',(-25.9420931202541,25.7101658109076,-44.0822570790823));
#21059=CARTESIAN_POINT('Ctrl Pts',(-25.9378877511288,25.7148139361769,-44.0826420445012));
#21060=CARTESIAN_POINT('Ctrl Pts',(-25.9357151027817,25.7172080773116,-44.082840754887));
#21061=CARTESIAN_POINT('Ctrl Pts',(-25.9298291560608,25.7236744933328,-44.0833786086417));
#21062=CARTESIAN_POINT('Ctrl Pts',(-25.926109020974,25.7277405055549,-44.0837180427182));
#21063=CARTESIAN_POINT('Ctrl Pts',(-25.9122732346699,25.7427849978114,-44.0849785879073));
#21064=CARTESIAN_POINT('Ctrl Pts',(-25.9020918902868,25.7537025618919,-44.0859025068547));
#21065=CARTESIAN_POINT('Ctrl Pts',(-25.7249126951009,25.9410667050012,-44.10191929494));
#21066=CARTESIAN_POINT('Ctrl Pts',(-25.5386029604331,26.0981055208699,-44.1179163434642));
#21067=CARTESIAN_POINT('Ctrl Pts',(-25.2694125362097,26.2773566600447,-44.139741262783));
#21068=CARTESIAN_POINT('Ctrl Pts',(-25.2007050358146,26.3194788565966,-44.1452046211406));
#21069=CARTESIAN_POINT('Ctrl Pts',(-25.0563156160717,26.4007148344623,-44.156401997556));
#21070=CARTESIAN_POINT('Ctrl Pts',(-24.9805117191027,26.4394948642049,-44.1621297489368));
#21071=CARTESIAN_POINT('Ctrl Pts',(-24.8420217959087,26.5035561143908,-44.1722350791115));
#21072=CARTESIAN_POINT('Ctrl Pts',(-24.7799058072096,26.5299545412802,-44.1766437670589));
#21073=CARTESIAN_POINT('Ctrl Pts',(-24.6992215948731,26.5612908082457,-44.1821740004241));
#21074=CARTESIAN_POINT('Ctrl Pts',(-24.6813792770177,26.568038762912,-44.1833848449165));
#21075=CARTESIAN_POINT('Ctrl Pts',(-24.6525719671542,26.5786422806434,-44.1853192115192));
#21076=CARTESIAN_POINT('Ctrl Pts',(-24.6416444914597,26.582597533392,-44.1860482387957));
#21077=CARTESIAN_POINT('Ctrl Pts',(-24.6283427683745,26.5873309372046,-44.1869297137504));
#21078=CARTESIAN_POINT('Ctrl Pts',(-24.6259888917026,26.5881654803317,-44.1870854740507));
#21079=CARTESIAN_POINT('Ctrl Pts',(-24.6214402312325,26.5897722121947,-44.1873860279881));
#21080=CARTESIAN_POINT('Ctrl Pts',(-24.6192455777557,26.5905447616199,-44.1875308430383));
#21081=CARTESIAN_POINT('Ctrl Pts',(-24.6152883148327,26.5919329601594,-44.1877916066426));
#21082=CARTESIAN_POINT('Ctrl Pts',(-24.6135260111995,26.5925494527908,-44.1879076055729));
#21083=CARTESIAN_POINT('Ctrl Pts',(-24.6097367155983,26.5938713371232,-44.1881567504995));
#21084=CARTESIAN_POINT('Ctrl Pts',(-24.6077095600623,26.5945762335898,-44.1882898664103));
#21085=CARTESIAN_POINT('Ctrl Pts',(-24.6022489584266,26.5964689192764,-44.1886479933995));
#21086=CARTESIAN_POINT('Ctrl Pts',(-24.5988141924936,26.5976529329612,-44.1888727788367));
#21087=CARTESIAN_POINT('Ctrl Pts',(-24.5830174690146,26.6030684235343,-44.1899044112115));
#21088=CARTESIAN_POINT('Ctrl Pts',(-24.5706316231403,26.6072305834148,-44.190707184202));
#21089=CARTESIAN_POINT('Ctrl Pts',(-24.3529866087256,26.6788981979001,-44.2047123418067));
#21090=CARTESIAN_POINT('Ctrl Pts',(-24.1414395626157,26.7256792846855,-44.2167701713485));
#21091=CARTESIAN_POINT('Ctrl Pts',(-23.7642556063533,26.7700502779302,-44.2379933954064));
#21092=CARTESIAN_POINT('Ctrl Pts',(-23.6005244821389,26.7767619929972,-44.2471175930084));
#21093=CARTESIAN_POINT('Ctrl Pts',(-23.3318620279809,26.7673150131332,-44.2626357384577));
#21094=CARTESIAN_POINT('Ctrl Pts',(-23.2269768729407,26.7584724148352,-44.2688281660583));
#21095=CARTESIAN_POINT('Ctrl Pts',(-23.1011371574599,26.741629517725,-44.2765016065565));
#21096=CARTESIAN_POINT('Ctrl Pts',(-23.0795854805883,26.7385223096761,-44.277824364355));
#21097=CARTESIAN_POINT('Ctrl Pts',(-23.053590284159,26.7345051437122,-44.2794307099017));
#21098=CARTESIAN_POINT('Ctrl Pts',(-23.049114702704,26.7338038445044,-44.279707663284));
#21099=CARTESIAN_POINT('Ctrl Pts',(-23.0404725949796,26.7324309977076,-44.2802432043376));
#21100=CARTESIAN_POINT('Ctrl Pts',(-23.0363058776558,26.7317606976387,-44.2805017519178));
#21101=CARTESIAN_POINT('Ctrl Pts',(-23.0291406774643,26.7305935881853,-44.2809469485592));
#21102=CARTESIAN_POINT('Ctrl Pts',(-23.0261415513006,26.7301007168043,-44.2811334721052));
#21103=CARTESIAN_POINT('Ctrl Pts',(-23.0199652520881,26.7290767388683,-44.2815179616249));
#21104=CARTESIAN_POINT('Ctrl Pts',(-23.0167881698206,26.7285451100312,-44.2817159440528));
#21105=CARTESIAN_POINT('Ctrl Pts',(-23.0091394957951,26.727253447292,-44.2821930648784));
#21106=CARTESIAN_POINT('Ctrl Pts',(-23.0046687097978,26.726488736432,-44.2824723520327));
#21107=CARTESIAN_POINT('Ctrl Pts',(-22.9909463680264,26.7241117548851,-44.2833308198402));
#21108=CARTESIAN_POINT('Ctrl Pts',(-22.9817002951605,26.7224684929247,-44.2839109874938));
#21109=CARTESIAN_POINT('Ctrl Pts',(-22.947640556665,26.7162615202366,-44.2860546331614));
#21110=CARTESIAN_POINT('Ctrl Pts',(-22.9228740627714,26.711446974669,-44.2876260954237));
#21111=CARTESIAN_POINT('Ctrl Pts',(-22.8922636534636,26.7051225033921,-44.2895845807344));
#21112=CARTESIAN_POINT('Ctrl Pts',(-22.8863635684173,26.7038862050682,-44.2899628229004));
#21113=CARTESIAN_POINT('Ctrl Pts',(-22.8737533468999,26.7012069146758,-44.2907728478956));
#21114=CARTESIAN_POINT('Ctrl Pts',(-22.8670442910972,26.6997590278718,-44.2912047845563));
#21115=CARTESIAN_POINT('Ctrl Pts',(-22.8587964581718,26.6979514622926,-44.2917369974765));
#21116=CARTESIAN_POINT('Ctrl Pts',(-22.8572532143058,26.6976120607894,-44.2918366313904));
#21117=CARTESIAN_POINT('Ctrl Pts',(-22.8529687294189,26.6966664814866,-44.2921133883212));
#21118=CARTESIAN_POINT('Ctrl Pts',(-22.8502280347373,26.6960578575121,-44.2922905885265));
#21119=CARTESIAN_POINT('Ctrl Pts',(-22.8343836352574,26.692517572628,-44.2933159655243));
#21120=CARTESIAN_POINT('Ctrl Pts',(-22.8212977139485,26.689507655021,-44.2941666019462));
#21121=CARTESIAN_POINT('Ctrl Pts',(-22.8043610757859,26.685500418919,-44.2952724825394));
#21122=CARTESIAN_POINT('Ctrl Pts',(-22.8004927226181,26.6845775956935,-44.2955254015406));
#21123=CARTESIAN_POINT('Ctrl Pts',(-22.7917864137743,26.6824836036253,-44.2960953876416));
#21124=CARTESIAN_POINT('Ctrl Pts',(-22.7869494512413,26.6813083834694,-44.2964125795543));
#21125=CARTESIAN_POINT('Ctrl Pts',(-22.7672935746408,26.676484408575,-44.2977036846719));
#21126=CARTESIAN_POINT('Ctrl Pts',(-22.7524981257123,26.6727416624544,-44.2986804777368));
#21127=CARTESIAN_POINT('Ctrl Pts',(-22.5923816023055,26.6310253314078,-44.3093051795325));
#21128=CARTESIAN_POINT('Ctrl Pts',(-22.4498757888398,26.5830464593163,-44.3192564266551));
#21129=CARTESIAN_POINT('Ctrl Pts',(-22.2310392747397,26.4919091114387,-44.3352088536775));
#21130=CARTESIAN_POINT('Ctrl Pts',(-22.1522381483177,26.4552849687086,-44.3410963813956));
#21131=CARTESIAN_POINT('Ctrl Pts',(-22.0750358850059,26.4155367074495,-44.3469709746179));
#21132=CARTESIAN_POINT('Ctrl Pts',(-22.0750360439056,26.4155367892604,-44.590879968079));
#21133=CARTESIAN_POINT('Ctrl Pts',(-22.0939080709219,26.4252532162916,-44.5894652751221));
#21134=CARTESIAN_POINT('Ctrl Pts',(-22.1128785974627,26.4347844837046,-44.588055277812));
#21135=CARTESIAN_POINT('Ctrl Pts',(-22.2024727047585,26.4786951348385,-44.5814568536133));
#21136=CARTESIAN_POINT('Ctrl Pts',(-22.2742473122324,26.5106747138146,-44.5763462405824));
#21137=CARTESIAN_POINT('Ctrl Pts',(-22.3614803433788,26.5457788114761,-44.5704007074401));
#21138=CARTESIAN_POINT('Ctrl Pts',(-22.3758774018533,26.5514523061039,-44.5694279513745));
#21139=CARTESIAN_POINT('Ctrl Pts',(-22.393785436603,26.5583607837284,-44.5682289883443));
#21140=CARTESIAN_POINT('Ctrl Pts',(-22.397258102119,26.5596935501703,-44.5679970012262));
#21141=CARTESIAN_POINT('Ctrl Pts',(-22.4027364778163,26.5617852091252,-44.5676318402594));
#21142=CARTESIAN_POINT('Ctrl Pts',(-22.4047406375414,26.5625481117396,-44.5674984247915));
#21143=CARTESIAN_POINT('Ctrl Pts',(-22.4084913993002,26.5639715905979,-44.5672490624772));
#21144=CARTESIAN_POINT('Ctrl Pts',(-22.4102378021263,26.5646326447256,-44.5671330873654));
#21145=CARTESIAN_POINT('Ctrl Pts',(-22.4141640654205,26.5661149266703,-44.5668726459375));
#21146=CARTESIAN_POINT('Ctrl Pts',(-22.4163442376663,26.5669353074364,-44.5667282313953));
#21147=CARTESIAN_POINT('Ctrl Pts',(-22.4218956069895,26.569017373432,-44.5663610211165));
#21148=CARTESIAN_POINT('Ctrl Pts',(-22.4252680419937,26.5702757795291,-44.566138422687));
#21149=CARTESIAN_POINT('Ctrl Pts',(-22.4439943671323,26.5772276873519,-44.5649050136516));
#21150=CARTESIAN_POINT('Ctrl Pts',(-22.4593897344955,26.5828098854831,-44.5639007885651));
#21151=CARTESIAN_POINT('Ctrl Pts',(-22.7748517307943,26.6944798336812,-44.543510098824));
#21152=CARTESIAN_POINT('Ctrl Pts',(-23.0890093136093,26.7556770305349,-44.5265119161997));
#21153=CARTESIAN_POINT('Ctrl Pts',(-23.5826415731307,26.7776274072564,-44.4985216854913));
#21154=CARTESIAN_POINT('Ctrl Pts',(-23.7585134945245,26.7710616324607,-44.4883279238951));
#21155=CARTESIAN_POINT('Ctrl Pts',(-23.9410319873616,26.7492328525504,-44.4771513848425));
#21156=CARTESIAN_POINT('Ctrl Pts',(-23.9491017435406,26.7482367374884,-44.4766560501961));
#21157=CARTESIAN_POINT('Ctrl Pts',(-23.962004530246,26.74659444539,-44.4758621326672));
#21158=CARTESIAN_POINT('Ctrl Pts',(-23.9668400497666,26.7459678157792,-44.4755641671165));
#21159=CARTESIAN_POINT('Ctrl Pts',(-23.9760452796345,26.7447536723811,-44.4749961075253));
#21160=CARTESIAN_POINT('Ctrl Pts',(-23.9804152464805,26.7441681599708,-44.4747260773252));
#21161=CARTESIAN_POINT('Ctrl Pts',(-23.9880851899923,26.7431244717508,-44.4742515017066));
#21162=CARTESIAN_POINT('Ctrl Pts',(-23.9913856906121,26.7426701419453,-44.4740470784323));
#21163=CARTESIAN_POINT('Ctrl Pts',(-23.9978318735311,26.741772606366,-44.4736474166093));
#21164=CARTESIAN_POINT('Ctrl Pts',(-24.0009776177882,26.741329865592,-44.4734521930138));
#21165=CARTESIAN_POINT('Ctrl Pts',(-24.0084473419851,26.7402672901807,-44.4729881755901));
#21166=CARTESIAN_POINT('Ctrl Pts',(-24.0127707187578,26.7396433151954,-44.4727192506367));
#21167=CARTESIAN_POINT('Ctrl Pts',(-24.0280263114848,26.7374098672805,-44.4717690420173));
#21168=CARTESIAN_POINT('Ctrl Pts',(-24.0389514098522,26.7357529740163,-44.4710862546508));
#21169=CARTESIAN_POINT('Ctrl Pts',(-24.1890481373595,26.7121990784579,-44.461673380567));
#21170=CARTESIAN_POINT('Ctrl Pts',(-24.3266266071022,26.6812586436298,-44.4526534228665));
#21171=CARTESIAN_POINT('Ctrl Pts',(-24.6115447361728,26.5972467807794,-44.4331197079007));
#21172=CARTESIAN_POINT('Ctrl Pts',(-24.7579434283226,26.5422402306996,-44.4225734931525));
#21173=CARTESIAN_POINT('Ctrl Pts',(-24.9714475392082,26.4437889976112,-44.4066583802809));
#21174=CARTESIAN_POINT('Ctrl Pts',(-25.0418928578784,26.4081115497507,-44.4013164795713));
#21175=CARTESIAN_POINT('Ctrl Pts',(-25.2237970862564,26.3074249545266,-44.3873790050684));
#21176=CARTESIAN_POINT('Ctrl Pts',(-25.3328005342051,26.2382410863217,-44.3788766457892));
#21177=CARTESIAN_POINT('Ctrl Pts',(-25.4438555731693,26.1580195816999,-44.370274693111));
#21178=CARTESIAN_POINT('Ctrl Pts',(-25.4503183301819,26.1533144653481,-44.3697743516584));
#21179=CARTESIAN_POINT('Ctrl Pts',(-25.4591185747322,26.1468573387428,-44.3690934514519));
#21180=CARTESIAN_POINT('Ctrl Pts',(-25.4614712158099,26.1451261771537,-44.3689114608231));
#21181=CARTESIAN_POINT('Ctrl Pts',(-25.4654044235199,26.1422237243919,-44.3686072755992));
#21182=CARTESIAN_POINT('Ctrl Pts',(-25.4669862710729,26.1410541846417,-44.3684849585616));
#21183=CARTESIAN_POINT('Ctrl Pts',(-25.4701001646737,26.1387475131164,-44.3682442153143));
#21184=CARTESIAN_POINT('Ctrl Pts',(-25.4716322718291,26.1376104692315,-44.3681257832574));
#21185=CARTESIAN_POINT('Ctrl Pts',(-25.4750088352727,26.1350999203895,-44.3678648146011));
#21186=CARTESIAN_POINT('Ctrl Pts',(-25.4768528361952,26.133725798013,-44.3677223214244));
#21187=CARTESIAN_POINT('Ctrl Pts',(-25.4832930663349,26.1289159032263,-44.3672247458874));
#21188=CARTESIAN_POINT('Ctrl Pts',(-25.487881623635,26.1254698032097,-44.3668703853822));
#21189=CARTESIAN_POINT('Ctrl Pts',(-25.5343508780332,26.0903759306731,-44.3632829921509));
#21190=CARTESIAN_POINT('Ctrl Pts',(-25.5754645642451,26.0577194076122,-44.3601196709919));
#21191=CARTESIAN_POINT('Ctrl Pts',(-25.623976105572,26.0172147386756,-44.3563751719887));
#21192=CARTESIAN_POINT('Ctrl Pts',(-25.6321532660555,26.010317841633,-44.3557435742859));
#21193=CARTESIAN_POINT('Ctrl Pts',(-25.7773001512882,25.8866539581371,-44.3445219058685));
#21194=CARTESIAN_POINT('Ctrl Pts',(-25.9042986776505,25.7586438255213,-44.3345205643541));
#21195=CARTESIAN_POINT('Ctrl Pts',(-26.1171650045232,25.5047280966557,-44.3160049273764));
#21196=CARTESIAN_POINT('Ctrl Pts',(-26.2060855198365,25.3820716587437,-44.3075312779911));
#21197=CARTESIAN_POINT('Ctrl Pts',(-26.3279667414487,25.1863175570599,-44.2941939611924));
#21198=CARTESIAN_POINT('Ctrl Pts',(-26.367375799719,25.117485771569,-44.2895385493286));
#21199=CARTESIAN_POINT('Ctrl Pts',(-26.422874155559,25.0116826216806,-44.2823876951746));
#21200=CARTESIAN_POINT('Ctrl Pts',(-26.440875565869,24.9757458333644,-44.2799598988517));
#21201=CARTESIAN_POINT('Ctrl Pts',(-26.4614231750913,24.932735431567,-44.2770522040719));
#21202=CARTESIAN_POINT('Ctrl Pts',(-26.4646232113001,24.9259767132744,-44.2765952283441));
#21203=CARTESIAN_POINT('Ctrl Pts',(-26.469510454303,24.9155609086803,-44.2758908781075));
#21204=CARTESIAN_POINT('Ctrl Pts',(-26.4712143923038,24.9119116636408,-44.27564408396));
#21205=CARTESIAN_POINT('Ctrl Pts',(-26.4743065046176,24.9052569176684,-44.27519399018));
#21206=CARTESIAN_POINT('Ctrl Pts',(-26.4756968988445,24.902252449282,-44.2749907677016));
#21207=CARTESIAN_POINT('Ctrl Pts',(-26.4785015903821,24.8961672778013,-44.2745791330657));
#21208=CARTESIAN_POINT('Ctrl Pts',(-26.4799156612509,24.8930864755126,-44.2743707134046));
#21209=CARTESIAN_POINT('Ctrl Pts',(-26.4839407810036,24.8842804228967,-44.2737749218644));
#21210=CARTESIAN_POINT('Ctrl Pts',(-26.4865399152792,24.8785497720521,-44.2733871397327));
#21211=CARTESIAN_POINT('Ctrl Pts',(-26.4976221638633,24.8539238132396,-44.2717204464071));
#21212=CARTESIAN_POINT('Ctrl Pts',(-26.5059396468539,24.8349549112277,-44.2704358587337));
#21213=CARTESIAN_POINT('Ctrl Pts',(-26.6537554979134,24.4888102377743,-44.2469768269609));
#21214=CARTESIAN_POINT('Ctrl Pts',(-26.7382953999085,24.140901122623,-44.2226997416912));
#21215=CARTESIAN_POINT('Ctrl Pts',(-26.770140375584,23.7074329332471,-44.1935053817704));
#21216=CARTESIAN_POINT('Ctrl Pts',(-26.7730299190195,23.6282965878572,-44.1882362982356));
#21217=CARTESIAN_POINT('Ctrl Pts',(-26.7730005616036,23.5440366669574,-44.1827398891842));
#21218=CARTESIAN_POINT('Ctrl Pts',(-26.7729867141529,23.5389436382277,-44.1824081078875));
#21219=CARTESIAN_POINT('Ctrl Pts',(-26.7729169771423,23.525241440422,-44.1815167226417));
#21220=CARTESIAN_POINT('Ctrl Pts',(-26.7728386624681,23.5166323677089,-44.1809579765281));
#21221=CARTESIAN_POINT('Ctrl Pts',(-26.7727004529541,23.5060856473388,-44.1802751583279));
#21222=CARTESIAN_POINT('Ctrl Pts',(-26.7726733084472,23.504147689381,-44.1801497603201));
#21223=CARTESIAN_POINT('Ctrl Pts',(-26.7719593807288,23.4562621398112,-44.1770530067836));
#21224=CARTESIAN_POINT('Ctrl Pts',(-26.7702916363931,23.4103313920859,-44.1741222338254));
#21225=CARTESIAN_POINT('Ctrl Pts',(-26.7673545128391,23.3594718680321,-44.1709323058993));
#21226=CARTESIAN_POINT('Ctrl Pts',(-26.76705552291,23.3544951941257,-44.1706207557786));
#21227=CARTESIAN_POINT('Ctrl Pts',(-26.7665915023988,23.3470598647845,-44.1701561887559));
#21228=CARTESIAN_POINT('Ctrl Pts',(-26.7664352005285,23.3446007017767,-44.170002684877));
#21229=CARTESIAN_POINT('Ctrl Pts',(-26.7661613664911,23.3403690298846,-44.1697387949705));
#21230=CARTESIAN_POINT('Ctrl Pts',(-26.7660451892934,23.3385964393573,-44.1696283323728));
#21231=CARTESIAN_POINT('Ctrl Pts',(-26.7658018452044,23.3349300350442,-44.1694000141655));
#21232=CARTESIAN_POINT('Ctrl Pts',(-26.765674471066,23.3330362408672,-44.1692821710267));
#21233=CARTESIAN_POINT('Ctrl Pts',(-26.76537091793,23.3285818008578,-44.1690051971424));
#21234=CARTESIAN_POINT('Ctrl Pts',(-26.7651933523251,23.3260212440186,-44.168846145083));
#21235=CARTESIAN_POINT('Ctrl Pts',(-26.7646042467549,23.317670701931,-44.1683279600743));
#21236=CARTESIAN_POINT('Ctrl Pts',(-26.7641801200287,23.311881573237,-44.1679695349507));
#21237=CARTESIAN_POINT('Ctrl Pts',(-26.7534026977402,23.1700349876353,-44.1592065764107));
#21238=CARTESIAN_POINT('Ctrl Pts',(-26.734432811212,23.0347499129251,-44.1512813715373));
#21239=CARTESIAN_POINT('Ctrl Pts',(-26.634435542464,22.5485165809761,-44.1230809506669));
#21240=CARTESIAN_POINT('Ctrl Pts',(-26.5034047872842,22.2106413311036,-44.1037060853067));
#21241=CARTESIAN_POINT('Ctrl Pts',(-26.3088087132513,21.8838485870156,-44.0807052283262));
#21242=CARTESIAN_POINT('Ctrl Pts',(-26.2981977652514,21.8664083354568,-44.079464753495));
#21243=CARTESIAN_POINT('Ctrl Pts',(-26.2841191877998,21.8437561740551,-44.0778361073457));
#21244=CARTESIAN_POINT('Ctrl Pts',(-26.2808008987597,21.8384516302325,-44.0774534582676));
#21245=CARTESIAN_POINT('Ctrl Pts',(-26.275664901501,21.8302942707367,-44.0768630564061));
#21246=CARTESIAN_POINT('Ctrl Pts',(-26.2738581012997,21.8274345767124,-44.0766557086453));
#21247=CARTESIAN_POINT('Ctrl Pts',(-26.2702567076883,21.8217543334991,-44.0762431068013));
#21248=CARTESIAN_POINT('Ctrl Pts',(-26.268462221066,21.8189337213476,-44.0760378568659));
#21249=CARTESIAN_POINT('Ctrl Pts',(-26.2644826113276,21.8126999247376,-44.0755834233583));
#21250=CARTESIAN_POINT('Ctrl Pts',(-26.262295434747,21.8092880636795,-44.0753341634085));
#21251=CARTESIAN_POINT('Ctrl Pts',(-26.2559904048339,21.7994933185549,-44.0746170274513));
#21252=CARTESIAN_POINT('Ctrl Pts',(-26.2518564337723,21.7931208874432,-44.0741485490933));
#21253=CARTESIAN_POINT('Ctrl Pts',(-26.2244425678996,21.7511884182704,-44.0710531028079));
#21254=CARTESIAN_POINT('Ctrl Pts',(-26.2004846114187,21.716078690838,-44.068400697592));
#21255=CARTESIAN_POINT('Ctrl Pts',(-26.127985994073,21.6142209958959,-44.0605204588349));
#21256=CARTESIAN_POINT('Ctrl Pts',(-26.0775707774778,21.5488559088993,-44.0552217598652));
#21257=CARTESIAN_POINT('Ctrl Pts',(-25.8333490901618,21.2561739553779,-44.0303464685409));
#21258=CARTESIAN_POINT('Ctrl Pts',(-25.6110809087874,21.0546022860257,-44.0096746401498));
#21259=CARTESIAN_POINT('Ctrl Pts',(-25.2904641200018,20.8362601068329,-43.9840249187697));
#21260=CARTESIAN_POINT('Ctrl Pts',(-25.2145923435694,20.7890810955855,-43.9782288179988));
#21261=CARTESIAN_POINT('Ctrl Pts',(-25.1312783365336,20.7419583953759,-43.9722283849153));
#21262=CARTESIAN_POINT('Ctrl Pts',(-25.1256962377857,20.7388230585876,-43.971828059682));
#21263=CARTESIAN_POINT('Ctrl Pts',(-25.1179424014397,20.7344982516968,-43.9712743909393));
#21264=CARTESIAN_POINT('Ctrl Pts',(-25.1157786286348,20.7332946454408,-43.9711201439557));
#21265=CARTESIAN_POINT('Ctrl Pts',(-25.1120573262834,20.731230269832,-43.9708553142887));
#21266=CARTESIAN_POINT('Ctrl Pts',(-25.1105004712808,20.7303682971328,-43.9707446537968));
#21267=CARTESIAN_POINT('Ctrl Pts',(-25.1072832510673,20.7285905220069,-43.9705162541773));
#21268=CARTESIAN_POINT('Ctrl Pts',(-25.105622794694,20.7276748971597,-43.9703985270504));
#21269=CARTESIAN_POINT('Ctrl Pts',(-25.1017228159079,20.7255288196915,-43.9701223747253));
#21270=CARTESIAN_POINT('Ctrl Pts',(-25.0994826305223,20.7242995609351,-43.9699640268711));
#21271=CARTESIAN_POINT('Ctrl Pts',(-25.0923242656936,20.7203826156539,-43.9694589121017));
#21272=CARTESIAN_POINT('Ctrl Pts',(-25.0874005016209,20.7177050750432,-43.9691127950465));
#21273=CARTESIAN_POINT('Ctrl Pts',(-25.0758334850618,20.7114539796289,-43.968302716921));
#21274=CARTESIAN_POINT('Ctrl Pts',(-25.0691845881576,20.7078908596037,-43.9678394063338));
#21275=CARTESIAN_POINT('Ctrl Pts',(-24.998481256975,20.6703201379484,-43.9629367112537));
#21276=CARTESIAN_POINT('Ctrl Pts',(-24.9333031374764,20.6384575685772,-43.9586263181298));
#21277=CARTESIAN_POINT('Ctrl Pts',(-24.7944778716177,20.5763070307247,-43.9497624106067));
#21278=CARTESIAN_POINT('Ctrl Pts',(-24.7206727173662,20.5464938034426,-43.9452287928722));
#21279=CARTESIAN_POINT('Ctrl Pts',(-24.383733114627,20.4246962089417,-43.9250168060919));
#21280=CARTESIAN_POINT('Ctrl Pts',(-24.1104678493923,20.3643543338467,-43.9098104778768));
#21281=CARTESIAN_POINT('Ctrl Pts',(-23.7604754597425,20.3335458310424,-43.8891203309641));
#21282=CARTESIAN_POINT('Ctrl Pts',(-23.6879147657029,20.3296247159069,-43.8847746886013));
#21283=CARTESIAN_POINT('Ctrl Pts',(-23.6058349411253,20.3279680086924,-43.8797747874892));
#21284=CARTESIAN_POINT('Ctrl Pts',(-23.5963815818106,20.3278188148966,-43.8791976867926));
#21285=CARTESIAN_POINT('Ctrl Pts',(-23.5824777448033,20.3276605774545,-43.8783470173325));
#21286=CARTESIAN_POINT('Ctrl Pts',(-23.5780276258794,20.3276191501693,-43.8780744654394));
#21287=CARTESIAN_POINT('Ctrl Pts',(-23.5701809476437,20.327562357695,-43.8775933835428));
#21288=CARTESIAN_POINT('Ctrl Pts',(-23.5667844159003,20.327543144235,-43.8773849746575));
#21289=CARTESIAN_POINT('Ctrl Pts',(-23.5597694582857,20.3275145523151,-43.8769541948769));
#21290=CARTESIAN_POINT('Ctrl Pts',(-23.5561510356956,20.3275058982921,-43.8767318015334));
#21291=CARTESIAN_POINT('Ctrl Pts',(-23.5469030809893,20.3274993553895,-43.8761629185265));
#21292=CARTESIAN_POINT('Ctrl Pts',(-23.541273572088,20.3275101231479,-43.8758161575446));
#21293=CARTESIAN_POINT('Ctrl Pts',(-23.5187936219518,20.3276120234177,-43.8744295827964));
#21294=CARTESIAN_POINT('Ctrl Pts',(-23.5019442172992,20.3278205622038,-43.8733860900485));
#21295=CARTESIAN_POINT('Ctrl Pts',(-23.2847025608547,20.3322134830783,-43.8598762763329));
#21296=CARTESIAN_POINT('Ctrl Pts',(-23.0851615594973,20.3549504286628,-43.8468109571785));
#21297=CARTESIAN_POINT('Ctrl Pts',(-22.655950357664,20.4449237468844,-43.8174216336159));
#21298=CARTESIAN_POINT('Ctrl Pts',(-22.428984400246,20.5194766173101,-43.8010244730725));
#21299=CARTESIAN_POINT('Ctrl Pts',(-22.2072485861976,20.6206640189016,-43.7851176388257));
#21300=CARTESIAN_POINT('Ctrl Pts',(-22.2021983029271,20.6229844795703,-43.7847554412038));
#21301=CARTESIAN_POINT('Ctrl Pts',(-22.1944923495493,20.626549316318,-43.7842029606378));
#21302=CARTESIAN_POINT('Ctrl Pts',(-22.1918323557627,20.6277842617501,-43.7840122839371));
#21303=CARTESIAN_POINT('Ctrl Pts',(-22.1858146767193,20.6305880582221,-43.7835809968639));
#21304=CARTESIAN_POINT('Ctrl Pts',(-22.1824579987125,20.6321590764513,-43.7833404795384));
#21305=CARTESIAN_POINT('Ctrl Pts',(-22.176432228506,20.634991985308,-43.7829088224254));
#21306=CARTESIAN_POINT('Ctrl Pts',(-22.1737621512612,20.636251757592,-43.7827175897463));
#21307=CARTESIAN_POINT('Ctrl Pts',(-22.1700524036658,20.6380082945575,-43.7824519528234));
#21308=CARTESIAN_POINT('Ctrl Pts',(-22.1690112710182,20.638501946572,-43.7823774087126));
#21309=CARTESIAN_POINT('Ctrl Pts',(-22.1651796896409,20.6403212045782,-43.7821030949611));
#21310=CARTESIAN_POINT('Ctrl Pts',(-22.1623908733598,20.6416502687856,-43.7819034822858));
#21311=CARTESIAN_POINT('Ctrl Pts',(-22.1582726146511,20.6436201760141,-43.7816087866479));
#21312=CARTESIAN_POINT('Ctrl Pts',(-22.1569417026505,20.6442579215438,-43.7815135601734));
#21313=CARTESIAN_POINT('Ctrl Pts',(-22.1532783696489,20.6460164102133,-43.7812514816206));
#21314=CARTESIAN_POINT('Ctrl Pts',(-22.1509468544462,20.6471390512311,-43.7810847185771));
#21315=CARTESIAN_POINT('Ctrl Pts',(-22.1131200866666,20.6654090623793,-43.7783797486821));
#21316=CARTESIAN_POINT('Ctrl Pts',(-22.0779389891969,20.6832044519755,-43.7758727072152));
#21317=CARTESIAN_POINT('Ctrl Pts',(-22.038869602058,20.7038755336643,-43.7731058153627));
#21318=CARTESIAN_POINT('Ctrl Pts',(-22.0346527949085,20.7061186013979,-43.7728074094154));
#21319=CARTESIAN_POINT('Ctrl Pts',(-22.0283145769239,20.7095082209585,-43.7723592416358));
#21320=CARTESIAN_POINT('Ctrl Pts',(-22.0261894644702,20.7106477802604,-43.7722090388073));
#21321=CARTESIAN_POINT('Ctrl Pts',(-22.0225132335267,20.7126244189981,-43.7719493118801));
#21322=CARTESIAN_POINT('Ctrl Pts',(-22.0209615230498,20.7134603856175,-43.7718397166471));
#21323=CARTESIAN_POINT('Ctrl Pts',(-22.0177319364094,20.7152037091745,-43.7716116865637));
#21324=CARTESIAN_POINT('Ctrl Pts',(-22.0160541818713,20.7161112817807,-43.7714932663394));
#21325=CARTESIAN_POINT('Ctrl Pts',(-22.0120729590632,20.7182694747473,-43.7712123549382));
#21326=CARTESIAN_POINT('Ctrl Pts',(-22.0097702021025,20.7195214203333,-43.7710499489061));
#21327=CARTESIAN_POINT('Ctrl Pts',(-22.0022314375228,20.7236319625877,-43.7705184994234));
#21328=CARTESIAN_POINT('Ctrl Pts',(-21.9970017996363,20.7265023100199,-43.770150205448));
#21329=CARTESIAN_POINT('Ctrl Pts',(-21.9846454581716,20.7333289447707,-43.7692808278358));
#21330=CARTESIAN_POINT('Ctrl Pts',(-21.9775256951463,20.7372978032738,-43.7687805297236));
#21331=CARTESIAN_POINT('Ctrl Pts',(-21.7124954253981,20.8863577236959,-43.7501781515924));
#21332=CARTESIAN_POINT('Ctrl Pts',(-21.4757280177946,21.0662832075499,-43.7342133350316));
#21333=CARTESIAN_POINT('Ctrl Pts',(-21.1243805163157,21.4190542105313,-43.7061904398073));
#21334=CARTESIAN_POINT('Ctrl Pts',(-20.9957130527506,21.5751143587977,-43.6945846522785));
#21335=CARTESIAN_POINT('Ctrl Pts',(-20.8754233831136,21.7525970129527,-43.6815560320951));
#21336=CARTESIAN_POINT('Ctrl Pts',(-20.8684152671212,21.7630689324418,-43.6807880545692));
#21337=CARTESIAN_POINT('Ctrl Pts',(-20.8589219557502,21.7774359488874,-43.6797353354369));
#21338=CARTESIAN_POINT('Ctrl Pts',(-20.8563833920705,21.7812957873085,-43.6794526017103));
#21339=CARTESIAN_POINT('Ctrl Pts',(-20.8520762541478,21.7878754825785,-43.6789707845249));
#21340=CARTESIAN_POINT('Ctrl Pts',(-20.850303466007,21.7905925842772,-43.67877185928));
#21341=CARTESIAN_POINT('Ctrl Pts',(-20.8468819488609,21.7958539891234,-43.6783867395101));
#21342=CARTESIAN_POINT('Ctrl Pts',(-20.8452327010549,21.798397951527,-43.6782005647097));
#21343=CARTESIAN_POINT('Ctrl Pts',(-20.8413268106732,21.804441448071,-43.6777583666986));
#21344=CARTESIAN_POINT('Ctrl Pts',(-20.8390733601025,21.8079430296312,-43.6775022247182));
#21345=CARTESIAN_POINT('Ctrl Pts',(-20.8325370248106,21.8181430667149,-43.6767562738232));
#21346=CARTESIAN_POINT('Ctrl Pts',(-20.8282721567674,21.8248529803659,-43.6762657954194));
#21347=CARTESIAN_POINT('Ctrl Pts',(-20.796666312334,21.8749872683819,-43.6726027207023));
#21348=CARTESIAN_POINT('Ctrl Pts',(-20.7703424755866,21.9190412151846,-43.6693927598346));
#21349=CARTESIAN_POINT('Ctrl Pts',(-20.6869628712055,22.0664642372666,-43.6586712095719));
#21350=CARTESIAN_POINT('Ctrl Pts',(-20.6345399322387,22.1723301948385,-43.6509999157526));
#21351=CARTESIAN_POINT('Ctrl Pts',(-20.5083899639432,22.466700413827,-43.6297791058253));
#21352=CARTESIAN_POINT('Ctrl Pts',(-20.4464093208745,22.6596568674107,-43.6159596054851));
#21353=CARTESIAN_POINT('Ctrl Pts',(-20.3732962817598,22.991647275081,-43.5931202175534));
#21354=CARTESIAN_POINT('Ctrl Pts',(-20.3523220606205,23.1279473593706,-43.5840087097376));
#21355=CARTESIAN_POINT('Ctrl Pts',(-20.3393984633464,23.2734800224228,-43.5748301915731));
#21356=CARTESIAN_POINT('Ctrl Pts',(-20.3386941987595,23.2817754415655,-43.5743089118939));
#21357=CARTESIAN_POINT('Ctrl Pts',(-20.3377740416975,23.2931359178994,-43.5735977115822));
#21358=CARTESIAN_POINT('Ctrl Pts',(-20.3375303835385,23.2961985989969,-43.573406245548));
#21359=CARTESIAN_POINT('Ctrl Pts',(-20.3371508927334,23.3010565016326,-43.573102978379));
#21360=CARTESIAN_POINT('Ctrl Pts',(-20.3370121848354,23.3028514867321,-43.5729910145659));
#21361=CARTESIAN_POINT('Ctrl Pts',(-20.3367456615726,23.3063385354253,-43.5727736882371));
#21362=CARTESIAN_POINT('Ctrl Pts',(-20.3366176793313,23.3080305723596,-43.5726683171305));
#21363=CARTESIAN_POINT('Ctrl Pts',(-20.3363131865703,23.3120989541871,-43.5724151585849));
#21364=CARTESIAN_POINT('Ctrl Pts',(-20.3361379752792,23.3144753933964,-43.5722674454976));
#21365=CARTESIAN_POINT('Ctrl Pts',(-20.3356432879058,23.3212880063699,-43.5718444530216));
#21366=CARTESIAN_POINT('Ctrl Pts',(-20.3353303576651,23.3257246723819,-43.5715695427246));
#21367=CARTESIAN_POINT('Ctrl Pts',(-20.3328454158035,23.362026323137,-43.5693246557309));
#21368=CARTESIAN_POINT('Ctrl Pts',(-20.3311379246294,23.3939227837029,-43.5673804288136));
#21369=CARTESIAN_POINT('Ctrl Pts',(-20.3267900776463,23.5064650668968,-43.5606034597468));
#21370=CARTESIAN_POINT('Ctrl Pts',(-20.3267039146096,23.5871846694168,-43.5558925417804));
#21371=CARTESIAN_POINT('Ctrl Pts',(-20.3363866708493,23.8524115641234,-43.5406623171468));
#21372=CARTESIAN_POINT('Ctrl Pts',(-20.3589814887923,24.036081615633,-43.5304950981702));
#21373=CARTESIAN_POINT('Ctrl Pts',(-20.4406325420954,24.4223202881182,-43.5083122289569));
#21374=CARTESIAN_POINT('Ctrl Pts',(-20.5040560283541,24.6230551518152,-43.496269887367));
#21375=CARTESIAN_POINT('Ctrl Pts',(-20.591615667434,24.828044369122,-43.4827274064666));
#21376=CARTESIAN_POINT('Ctrl Pts',(-20.5967556209701,24.8398804102354,-43.4819410435605));
#21377=CARTESIAN_POINT('Ctrl Pts',(-20.603850841636,24.8559540357782,-43.4808670002361));
#21378=CARTESIAN_POINT('Ctrl Pts',(-20.6057444836715,24.8602188258035,-43.4805814344464));
#21379=CARTESIAN_POINT('Ctrl Pts',(-20.6089756032406,24.8674534280129,-43.4800960019841));
#21380=CARTESIAN_POINT('Ctrl Pts',(-20.6103083368397,24.8704253620999,-43.479896298616));
#21381=CARTESIAN_POINT('Ctrl Pts',(-20.6128887940042,24.8761563760043,-43.4795106319443));
#21382=CARTESIAN_POINT('Ctrl Pts',(-20.6141359056584,24.8789157283209,-43.479324689909));
#21383=CARTESIAN_POINT('Ctrl Pts',(-20.6170951367739,24.885438794376,-43.4788845264711));
#21384=CARTESIAN_POINT('Ctrl Pts',(-20.6188106112326,24.8892009721269,-43.4786301895062));
#21385=CARTESIAN_POINT('Ctrl Pts',(-20.6237716985429,24.9000258130365,-43.4778970219368));
#21386=CARTESIAN_POINT('Ctrl Pts',(-20.6270356115475,24.9070800129527,-43.4774175591392));
#21387=CARTESIAN_POINT('Ctrl Pts',(-20.6496400968237,24.9554742667882,-43.4741166150031));
#21388=CARTESIAN_POINT('Ctrl Pts',(-20.6698306064827,24.9964094420536,-43.4712657185882));
#21389=CARTESIAN_POINT('Ctrl Pts',(-20.7328014883289,25.1175255684658,-43.4626475897631));
#21390=CARTESIAN_POINT('Ctrl Pts',(-20.7781078372217,25.1963346588691,-43.4567931385375));
#21391=CARTESIAN_POINT('Ctrl Pts',(-20.9295259028893,25.4357021377593,-43.4382293650395));
#21392=CARTESIAN_POINT('Ctrl Pts',(-21.0467155028626,25.5887365569703,-43.4251802510341));
#21393=CARTESIAN_POINT('Ctrl Pts',(-21.2778015911528,25.8403094039,-43.4020821930794));
#21394=CARTESIAN_POINT('Ctrl Pts',(-21.3862926052458,25.9430918478627,-43.3920532200363));
#21395=CARTESIAN_POINT('Ctrl Pts',(-21.5293854483496,26.0609329528217,-43.3801435272218));
#21396=CARTESIAN_POINT('Ctrl Pts',(-21.5576281680185,26.0834063690238,-43.3778517341946));
#21397=CARTESIAN_POINT('Ctrl Pts',(-21.5899358095286,26.1082395517465,-43.3753013482047));
#21398=CARTESIAN_POINT('Ctrl Pts',(-21.5936339172394,26.1110693631318,-43.3750104544027));
#21399=CARTESIAN_POINT('Ctrl Pts',(-21.599232033722,26.1153338651161,-43.3745716872008));
#21400=CARTESIAN_POINT('Ctrl Pts',(-21.6011275002128,26.1167744665936,-43.3744233981051));
#21401=CARTESIAN_POINT('Ctrl Pts',(-21.6044227614518,26.1192731907677,-43.3741660746582));
#21402=CARTESIAN_POINT('Ctrl Pts',(-21.605821823781,26.1203322704701,-43.3740569722799));
#21403=CARTESIAN_POINT('Ctrl Pts',(-21.6087485878461,26.1225440511554,-43.373829048276));
#21404=CARTESIAN_POINT('Ctrl Pts',(-21.6102764503374,26.1236965331939,-43.3737102425814));
#21405=CARTESIAN_POINT('Ctrl Pts',(-21.6139268696478,26.1264449828392,-43.373426810005));
#21406=CARTESIAN_POINT('Ctrl Pts',(-21.616050380609,26.1280396939121,-43.3732622724333));
#21407=CARTESIAN_POINT('Ctrl Pts',(-21.6231001782321,26.1333203246849,-43.3727171454003));
#21408=CARTESIAN_POINT('Ctrl Pts',(-21.6280350876932,26.1369947910035,-43.3723373595259));
#21409=CARTESIAN_POINT('Ctrl Pts',(-21.6397926060123,26.1456970523951,-43.3714367195191));
#21410=CARTESIAN_POINT('Ctrl Pts',(-21.6466246241101,26.1507121412347,-43.3709167292385));
#21411=CARTESIAN_POINT('Ctrl Pts',(-21.6709824950554,26.1684447660121,-43.3690743976062));
#21412=CARTESIAN_POINT('Ctrl Pts',(-21.6886170889714,26.1810128745784,-43.3677617624746));
#21413=CARTESIAN_POINT('Ctrl Pts',(-21.7302331169343,26.2100444274727,-43.3647099031045));
#21414=CARTESIAN_POINT('Ctrl Pts',(-21.7543137278452,26.2263630543977,-43.3629790235023));
#21415=CARTESIAN_POINT('Ctrl Pts',(-21.8104356227183,26.263296201581,-43.3590171334029));
#21416=CARTESIAN_POINT('Ctrl Pts',(-21.842628448613,26.2836732881986,-43.3567975297631));
#21417=CARTESIAN_POINT('Ctrl Pts',(-21.9404679187915,26.3431993746108,-43.3501860564257));
#21418=CARTESIAN_POINT('Ctrl Pts',(-22.0071309136415,26.3805752452119,-43.3458587578018));
#21419=CARTESIAN_POINT('Ctrl Pts',(-22.0750361136176,26.4155368251522,-43.341564988124));
#21420=CARTESIAN_POINT('Origin',(-23.5502525316942,23.5502525316942,-77.3107734492734));
#21421=CARTESIAN_POINT('',(-22.0750357700609,26.4155366482691,-41.8463063580885));
#21422=CARTESIAN_POINT('',(-22.0750360182176,26.4155367760347,-42.0958126606468));
#21423=CARTESIAN_POINT('',(-22.0750360153461,26.4155367745563,-77.3107734492734));
#21424=CARTESIAN_POINT('Ctrl Pts',(-22.0750357700609,26.4155366482691,-41.8463063580885));
#21425=CARTESIAN_POINT('Ctrl Pts',(-21.9772531459235,26.3651924030721,-41.8524539240125));
#21426=CARTESIAN_POINT('Ctrl Pts',(-21.8820641779325,26.3098512670906,-41.8586200916589));
#21427=CARTESIAN_POINT('Ctrl Pts',(-21.7018797839775,26.1923474161378,-41.8709105408599));
#21428=CARTESIAN_POINT('Ctrl Pts',(-21.6167745270493,26.1307189459993,-41.8770130351582));
#21429=CARTESIAN_POINT('Ctrl Pts',(-21.4973713426764,26.0350264255765,-41.8861354317059));
#21430=CARTESIAN_POINT('Ctrl Pts',(-21.4605854268994,26.0041705202263,-41.8890288970496));
#21431=CARTESIAN_POINT('Ctrl Pts',(-21.4185764649339,25.9673038142383,-41.8924372254398));
#21432=CARTESIAN_POINT('Ctrl Pts',(-21.4126682026131,25.9620802598644,-41.8929190375543));
#21433=CARTESIAN_POINT('Ctrl Pts',(-21.4037069666418,25.9540987468317,-41.8936535898197));
#21434=CARTESIAN_POINT('Ctrl Pts',(-21.4006399735063,25.9513565149293,-41.8939056682826));
#21435=CARTESIAN_POINT('Ctrl Pts',(-21.3953267190542,25.946587537054,-41.8943435496765));
#21436=CARTESIAN_POINT('Ctrl Pts',(-21.3930780400227,25.944563482318,-41.8945292387955));
#21437=CARTESIAN_POINT('Ctrl Pts',(-21.3884076157069,25.9403476742309,-41.8949156778006));
#21438=CARTESIAN_POINT('Ctrl Pts',(-21.3859863465828,25.938155400535,-41.8951164496235));
#21439=CARTESIAN_POINT('Ctrl Pts',(-21.3793646061916,25.9321415773189,-41.8956667119782));
#21440=CARTESIAN_POINT('Ctrl Pts',(-21.3751709111567,25.9283126137988,-41.8960165174593));
#21441=CARTESIAN_POINT('Ctrl Pts',(-21.3591627440885,25.9136189293234,-41.8973568478698));
#21442=CARTESIAN_POINT('Ctrl Pts',(-21.3474195336887,25.9026772286176,-41.8983506600611));
#21443=CARTESIAN_POINT('Ctrl Pts',(-21.1563529310658,25.7219663065232,-41.9146966355623));
#21444=CARTESIAN_POINT('Ctrl Pts',(-20.9970827748512,25.5322644302741,-41.9309845116944));
#21445=CARTESIAN_POINT('Ctrl Pts',(-20.769825700203,25.1881616169025,-41.9588311178608));
#21446=CARTESIAN_POINT('Ctrl Pts',(-20.6893758193029,25.0432050835991,-41.970113442863));
#21447=CARTESIAN_POINT('Ctrl Pts',(-20.5941299169304,24.8353357931206,-41.9852240713513));
#21448=CARTESIAN_POINT('Ctrl Pts',(-20.5695316750797,24.7772016815339,-41.9893397432001));
#21449=CARTESIAN_POINT('Ctrl Pts',(-20.539947288755,24.7011314864607,-41.9945514894867));
#21450=CARTESIAN_POINT('Ctrl Pts',(-20.5333881561239,24.6838262613359,-41.9957256797153));
#21451=CARTESIAN_POINT('Ctrl Pts',(-20.5230460552348,24.6558145635857,-41.9976068413836));
#21452=CARTESIAN_POINT('Ctrl Pts',(-20.5191700679046,24.6451431948922,-41.9983189611952));
#21453=CARTESIAN_POINT('Ctrl Pts',(-20.5142285853146,24.631310939241,-41.9992359572336));
#21454=CARTESIAN_POINT('Ctrl Pts',(-20.5131115532476,24.6281687440217,-41.999443862976));
#21455=CARTESIAN_POINT('Ctrl Pts',(-20.5113078476957,24.6230698833658,-41.9997805730516));
#21456=CARTESIAN_POINT('Ctrl Pts',(-20.5106181855329,24.6211142894133,-41.9999095560698));
#21457=CARTESIAN_POINT('Ctrl Pts',(-20.5093069448188,24.6173846854606,-42.000155244019));
#21458=CARTESIAN_POINT('Ctrl Pts',(-20.5086850354972,24.615610810412,-42.0002719680059));
#21459=CARTESIAN_POINT('Ctrl Pts',(-20.5072708046455,24.6115656606711,-42.0005378505535));
#21460=CARTESIAN_POINT('Ctrl Pts',(-20.5064794748299,24.6092940451811,-42.0006869491311));
#21461=CARTESIAN_POINT('Ctrl Pts',(-20.5040223867026,24.6022151502412,-42.0011509224828));
#21462=CARTESIAN_POINT('Ctrl Pts',(-20.5023654577852,24.5974047807082,-42.001465271605));
#21463=CARTESIAN_POINT('Ctrl Pts',(-20.4896787706626,24.5602877720829,-42.0038837237919));
#21464=CARTESIAN_POINT('Ctrl Pts',(-20.4791510409752,24.5278100977849,-42.0059585890049));
#21465=CARTESIAN_POINT('Ctrl Pts',(-20.4393291266002,24.3979619287134,-42.0141133862875));
#21466=CARTESIAN_POINT('Ctrl Pts',(-20.4141314820632,24.2993882418838,-42.0199927732055));
#21467=CARTESIAN_POINT('Ctrl Pts',(-20.3513205921513,23.9941354409259,-42.0377076206906));
#21468=CARTESIAN_POINT('Ctrl Pts',(-20.3292018707765,23.7848474238674,-42.0492072795638));
#21469=CARTESIAN_POINT('Ctrl Pts',(-20.3268140389264,23.4725158351821,-42.0669666502198));
#21470=CARTESIAN_POINT('Ctrl Pts',(-20.3309100057908,23.3701698817405,-42.0728749776811));
#21471=CARTESIAN_POINT('Ctrl Pts',(-20.3455751930156,23.2032486111865,-42.0827826772659));
#21472=CARTESIAN_POINT('Ctrl Pts',(-20.3532507868973,23.1384910873882,-42.0866933019996));
#21473=CARTESIAN_POINT('Ctrl Pts',(-20.3641371763042,23.0656306614346,-42.091183635963));
#21474=CARTESIAN_POINT('Ctrl Pts',(-20.365422855797,23.0572521784007,-42.0917013459963));
#21475=CARTESIAN_POINT('Ctrl Pts',(-20.3674006303901,23.0446941437229,-42.0924793706786));
#21476=CARTESIAN_POINT('Ctrl Pts',(-20.3680679435657,23.0405106792913,-42.0927388974333));
#21477=CARTESIAN_POINT('Ctrl Pts',(-20.369228551177,23.0333257963348,-42.0931852149236));
#21478=CARTESIAN_POINT('Ctrl Pts',(-20.3697178508434,23.0303237306508,-42.0933718783629));
#21479=CARTESIAN_POINT('Ctrl Pts',(-20.370733101384,23.0241497924835,-42.0937561320919));
#21480=CARTESIAN_POINT('Ctrl Pts',(-20.3712595502285,23.02097800596,-42.0939537380618));
#21481=CARTESIAN_POINT('Ctrl Pts',(-20.3725363974964,23.0133557982813,-42.0944290943114));
#21482=CARTESIAN_POINT('Ctrl Pts',(-20.3732913985376,23.0089061638473,-42.0947069909473));
#21483=CARTESIAN_POINT('Ctrl Pts',(-20.3756306592494,22.9952930659829,-42.0955584039115));
#21484=CARTESIAN_POINT('Ctrl Pts',(-20.3772452260908,22.9861349222681,-42.0961328852279));
#21485=CARTESIAN_POINT('Ctrl Pts',(-20.3961066341779,22.8817925776158,-42.1026977986869));
#21486=CARTESIAN_POINT('Ctrl Pts',(-20.4175892926568,22.7874335243588,-42.1088232591418));
#21487=CARTESIAN_POINT('Ctrl Pts',(-20.4595390820231,22.635181862189,-42.1190330845082));
#21488=CARTESIAN_POINT('Ctrl Pts',(-20.4774747040188,22.5766511419825,-42.1230384878416));
#21489=CARTESIAN_POINT('Ctrl Pts',(-20.5520754098858,22.3558546782773,-42.138443849064));
#21490=CARTESIAN_POINT('Ctrl Pts',(-20.6200179521351,22.1977105702668,-42.1501147494433));
#21491=CARTESIAN_POINT('Ctrl Pts',(-20.7812055735126,21.8923688109779,-42.1734514990341));
#21492=CARTESIAN_POINT('Ctrl Pts',(-20.8744360382992,21.7457521434629,-42.1850750385602));
#21493=CARTESIAN_POINT('Ctrl Pts',(-20.9853026803273,21.599032870359,-42.1966501638791));
#21494=CARTESIAN_POINT('Ctrl Pts',(-20.9916182186336,21.5907586261338,-42.1973026909872));
#21495=CARTESIAN_POINT('Ctrl Pts',(-20.9999481600588,21.5799541709706,-42.1981542628992));
#21496=CARTESIAN_POINT('Ctrl Pts',(-21.0019263463784,21.5773963099422,-42.1983558286606));
#21497=CARTESIAN_POINT('Ctrl Pts',(-21.0051652400162,21.573221311745,-42.1986847630483));
#21498=CARTESIAN_POINT('Ctrl Pts',(-21.0064236407612,21.571602400765,-42.1988122955204));
#21499=CARTESIAN_POINT('Ctrl Pts',(-21.0088428028075,21.568496312718,-42.1990569499474));
#21500=CARTESIAN_POINT('Ctrl Pts',(-21.010003321482,21.5670089582617,-42.1991740882795));
#21501=CARTESIAN_POINT('Ctrl Pts',(-21.0126752770312,21.5635906953627,-42.1994432652668));
#21502=CARTESIAN_POINT('Ctrl Pts',(-21.014187615828,21.5616604875767,-42.199595239177));
#21503=CARTESIAN_POINT('Ctrl Pts',(-21.0188771863956,21.5556892088956,-42.2000653180862));
#21504=CARTESIAN_POINT('Ctrl Pts',(-21.0220619049011,21.5516539869881,-42.2003828895237));
#21505=CARTESIAN_POINT('Ctrl Pts',(-21.048208529133,21.518687211093,-42.2029767545228));
#21506=CARTESIAN_POINT('Ctrl Pts',(-21.0716577896036,21.490143254738,-42.20521873646));
#21507=CARTESIAN_POINT('Ctrl Pts',(-21.0985907105131,21.4584845550575,-42.2077090886249));
#21508=CARTESIAN_POINT('Ctrl Pts',(-21.1015951965244,21.4549682529067,-42.20798574228));
#21509=CARTESIAN_POINT('Ctrl Pts',(-21.108136588268,21.4473458169412,-42.2085856012056));
#21510=CARTESIAN_POINT('Ctrl Pts',(-21.1116763086222,21.443242105251,-42.2089086408403));
#21511=CARTESIAN_POINT('Ctrl Pts',(-21.1219216727674,21.4314247266792,-42.2098392234232));
#21512=CARTESIAN_POINT('Ctrl Pts',(-21.1286537374724,21.423733941964,-42.2104452589701));
#21513=CARTESIAN_POINT('Ctrl Pts',(-21.1417117784353,21.4089587162792,-42.2116106374164));
#21514=CARTESIAN_POINT('Ctrl Pts',(-21.1480326944234,21.4018699723854,-42.2121702424001));
#21515=CARTESIAN_POINT('Ctrl Pts',(-21.1763833872309,21.3703569626046,-42.214660698649));
#21516=CARTESIAN_POINT('Ctrl Pts',(-21.1987555846416,21.3462421763196,-42.2165738573126));
#21517=CARTESIAN_POINT('Ctrl Pts',(-21.4028245425305,21.132923277902,-42.2336095192303));
#21518=CARTESIAN_POINT('Ctrl Pts',(-21.6066250754386,20.9662134490909,-42.247807610266));
#21519=CARTESIAN_POINT('Ctrl Pts',(-21.9418568106877,20.7543272299207,-42.2704712334115));
#21520=CARTESIAN_POINT('Ctrl Pts',(-22.0596781889589,20.6897776502195,-42.2783110418898));
#21521=CARTESIAN_POINT('Ctrl Pts',(-22.1939061139439,20.6267888557906,-42.2872750033166));
#21522=CARTESIAN_POINT('Ctrl Pts',(-22.2066803525832,20.6208960735144,-42.2881283122233));
#21523=CARTESIAN_POINT('Ctrl Pts',(-22.2290709151561,20.610744528428,-42.2896245671747));
#21524=CARTESIAN_POINT('Ctrl Pts',(-22.2386703302467,20.6064488205291,-42.2902662362333));
#21525=CARTESIAN_POINT('Ctrl Pts',(-22.2525233778769,20.6003308348388,-42.2911925643565));
#21526=CARTESIAN_POINT('Ctrl Pts',(-22.2567602483382,20.5984705806026,-42.2914759199633));
#21527=CARTESIAN_POINT('Ctrl Pts',(-22.2641291083669,20.5952540966387,-42.2919688201161));
#21528=CARTESIAN_POINT('Ctrl Pts',(-22.2672592810342,20.5938937020141,-42.2921782217));
#21529=CARTESIAN_POINT('Ctrl Pts',(-22.2732883196702,20.5912848188119,-42.292581602588));
#21530=CARTESIAN_POINT('Ctrl Pts',(-22.2761868718267,20.5900356107747,-42.2927755570157));
#21531=CARTESIAN_POINT('Ctrl Pts',(-22.2830289397769,20.5870987506503,-42.2932334451609));
#21532=CARTESIAN_POINT('Ctrl Pts',(-22.2869739923337,20.5854147125646,-42.2934975019409));
#21533=CARTESIAN_POINT('Ctrl Pts',(-22.3006726082262,20.5795994424533,-42.2944145613369));
#21534=CARTESIAN_POINT('Ctrl Pts',(-22.3104430882525,20.5755084584332,-42.2950689330862));
#21535=CARTESIAN_POINT('Ctrl Pts',(-22.4277489051545,20.5270698147462,-42.3029291912258));
#21536=CARTESIAN_POINT('Ctrl Pts',(-22.5375762724683,20.4885325361548,-42.3103311111154));
#21537=CARTESIAN_POINT('Ctrl Pts',(-22.663020889403,20.4520040386413,-42.3188452461836));
#21538=CARTESIAN_POINT('Ctrl Pts',(-22.6768327436961,20.4480820695106,-42.3197834027166));
#21539=CARTESIAN_POINT('Ctrl Pts',(-22.9133305712872,20.3826315354656,-42.3358589201773));
#21540=CARTESIAN_POINT('Ctrl Pts',(-23.1419572090988,20.3451369001051,-42.3516458422299));
#21541=CARTESIAN_POINT('Ctrl Pts',(-23.4456335415051,20.328370469413,-42.3721039806439));
#21542=CARTESIAN_POINT('Ctrl Pts',(-23.5187969997473,20.326825656299,-42.376987993387));
#21543=CARTESIAN_POINT('Ctrl Pts',(-23.6591955041478,20.3286424852505,-42.386205683276));
#21544=CARTESIAN_POINT('Ctrl Pts',(-23.7264001447948,20.331617196725,-42.3905497023721));
#21545=CARTESIAN_POINT('Ctrl Pts',(-23.804275611836,20.3375111299206,-42.3954674478925));
#21546=CARTESIAN_POINT('Ctrl Pts',(-23.8150793914783,20.3383836392505,-42.3961470879095));
#21547=CARTESIAN_POINT('Ctrl Pts',(-23.829141937261,20.3395907636404,-42.3970281532736));
#21548=CARTESIAN_POINT('Ctrl Pts',(-23.832404717011,20.3398758506911,-42.3972323264589));
#21549=CARTESIAN_POINT('Ctrl Pts',(-23.8377189687975,20.3403483503212,-42.3975644585424));
#21550=CARTESIAN_POINT('Ctrl Pts',(-23.8397706953569,20.3405327559157,-42.3976925873288));
#21551=CARTESIAN_POINT('Ctrl Pts',(-23.8436980708678,20.3408895379243,-42.3979376541969));
#21552=CARTESIAN_POINT('Ctrl Pts',(-23.8455737395852,20.3410615909078,-42.3980546099619));
#21553=CARTESIAN_POINT('Ctrl Pts',(-23.8498711169182,20.3414595839368,-42.3983223754822));
#21554=CARTESIAN_POINT('Ctrl Pts',(-23.852292726685,20.3416866216819,-42.3984731227273));
#21555=CARTESIAN_POINT('Ctrl Pts',(-23.8599177562962,20.34241021431,-42.3989473497799));
#21556=CARTESIAN_POINT('Ctrl Pts',(-23.8651202601746,20.3429166903765,-42.3992702699017));
#21557=CARTESIAN_POINT('Ctrl Pts',(-23.9075757440468,20.3471541278045,-42.4019004166495));
#21558=CARTESIAN_POINT('Ctrl Pts',(-23.944764296926,20.3515215290251,-42.40417239754));
#21559=CARTESIAN_POINT('Ctrl Pts',(-24.3039480142052,20.4000637401541,-42.4258801344396));
#21560=CARTESIAN_POINT('Ctrl Pts',(-24.617633056031,20.492064434711,-42.4431593496046));
#21561=CARTESIAN_POINT('Ctrl Pts',(-25.033682016491,20.6860777768977,-42.4693963282932));
#21562=CARTESIAN_POINT('Ctrl Pts',(-25.1514194910646,20.7501957829155,-42.4772205318204));
#21563=CARTESIAN_POINT('Ctrl Pts',(-25.2828093379547,20.8327507463927,-42.486601805105));
#21564=CARTESIAN_POINT('Ctrl Pts',(-25.3006881220055,20.8442325298096,-42.4878928141654));
#21565=CARTESIAN_POINT('Ctrl Pts',(-25.3235783791506,20.8592544635153,-42.4895649186859));
#21566=CARTESIAN_POINT('Ctrl Pts',(-25.3286953819097,20.8626334753739,-42.489939959418));
#21567=CARTESIAN_POINT('Ctrl Pts',(-25.3369097189948,20.8680915422372,-42.4905440402268));
#21568=CARTESIAN_POINT('Ctrl Pts',(-25.3400131587495,20.8701614183261,-42.4907727339081));
#21569=CARTESIAN_POINT('Ctrl Pts',(-25.3459069578501,20.8741071602081,-42.4912079429805));
#21570=CARTESIAN_POINT('Ctrl Pts',(-25.3486979909341,20.875982014805,-42.4914144199335));
#21571=CARTESIAN_POINT('Ctrl Pts',(-25.3550400611338,20.8802566693332,-42.491884470234));
#21572=CARTESIAN_POINT('Ctrl Pts',(-25.3585892499257,20.8826591884993,-42.4921481464711));
#21573=CARTESIAN_POINT('Ctrl Pts',(-25.3693463877062,20.8899722506675,-42.4929492183142));
#21574=CARTESIAN_POINT('Ctrl Pts',(-25.3765391607579,20.8949049505468,-42.4934874560171));
#21575=CARTESIAN_POINT('Ctrl Pts',(-25.4270751002638,20.9298642329007,-42.4972875788717));
#21576=CARTESIAN_POINT('Ctrl Pts',(-25.469693482917,20.9609198584305,-42.5005887754197));
#21577=CARTESIAN_POINT('Ctrl Pts',(-25.5148876366285,20.9955814407048,-42.5041983783339));
#21578=CARTESIAN_POINT('Ctrl Pts',(-25.5182412265592,20.9981639800784,-42.5044668860547));
#21579=CARTESIAN_POINT('Ctrl Pts',(-25.5247750204387,21.0032160740899,-42.504991311349));
#21580=CARTESIAN_POINT('Ctrl Pts',(-25.5279557044425,21.0056849976737,-42.5052472043932));
#21581=CARTESIAN_POINT('Ctrl Pts',(-25.5350326513094,21.0111995790706,-42.5058179007252));
#21582=CARTESIAN_POINT('Ctrl Pts',(-25.5389265415828,21.0142482530289,-42.506132819046));
#21583=CARTESIAN_POINT('Ctrl Pts',(-25.5569838986532,21.028453203817,-42.5075974406308));
#21584=CARTESIAN_POINT('Ctrl Pts',(-25.5710603904479,21.0397190810876,-42.5087513120912));
#21585=CARTESIAN_POINT('Ctrl Pts',(-25.6027457622187,21.065517066641,-42.5113763314517));
#21586=CARTESIAN_POINT('Ctrl Pts',(-25.6202961055793,21.0801192651444,-42.5128500655626));
#21587=CARTESIAN_POINT('Ctrl Pts',(-25.8682073367593,21.2908834682366,-42.5339509385485));
#21588=CARTESIAN_POINT('Ctrl Pts',(-26.0699644106634,21.5183414982037,-42.554851459151));
#21589=CARTESIAN_POINT('Ctrl Pts',(-26.2780933961966,21.8325396938435,-42.5798920261439));
#21590=CARTESIAN_POINT('Ctrl Pts',(-26.3170242708538,21.8959765357849,-42.5847687082337));
#21591=CARTESIAN_POINT('Ctrl Pts',(-26.3687342173936,21.9871772482324,-42.5914749978725));
#21592=CARTESIAN_POINT('Ctrl Pts',(-26.3833666073867,22.0138580005604,-42.5934014212401));
#21593=CARTESIAN_POINT('Ctrl Pts',(-26.3997375880703,22.0447383591887,-42.5955871226326));
#21594=CARTESIAN_POINT('Ctrl Pts',(-26.4018472153906,22.0487380393782,-42.595869380028));
#21595=CARTESIAN_POINT('Ctrl Pts',(-26.4050252235891,22.054794137042,-42.5962954764623));
#21596=CARTESIAN_POINT('Ctrl Pts',(-26.4060998049847,22.0568472671244,-42.5964397086933));
#21597=CARTESIAN_POINT('Ctrl Pts',(-26.408035838937,22.0605560476472,-42.5966998464624));
#21598=CARTESIAN_POINT('Ctrl Pts',(-26.4088980655487,22.0622112830827,-42.5968158012749));
#21599=CARTESIAN_POINT('Ctrl Pts',(-26.4107518733939,22.065777636598,-42.5970653235902));
#21600=CARTESIAN_POINT('Ctrl Pts',(-26.4117429747484,22.0676889943004,-42.5971988601585));
#21601=CARTESIAN_POINT('Ctrl Pts',(-26.4144147587184,22.0728542400324,-42.5975592121155));
#21602=CARTESIAN_POINT('Ctrl Pts',(-26.4160918178819,22.0761100145078,-42.5977857970638));
#21603=CARTESIAN_POINT('Ctrl Pts',(-26.4238538358473,22.0912421882877,-42.5988363833944));
#21604=CARTESIAN_POINT('Ctrl Pts',(-26.4298706572446,22.1031536743205,-42.5996561270869));
#21605=CARTESIAN_POINT('Ctrl Pts',(-26.4365067778225,22.1164964808641,-42.6005666974657));
#21606=CARTESIAN_POINT('Ctrl Pts',(-26.4371991066031,22.1178910339406,-42.6006617744745));
#21607=CARTESIAN_POINT('Ctrl Pts',(-26.5905687020566,22.4273852639512,-42.6217417220802));
#21608=CARTESIAN_POINT('Ctrl Pts',(-26.6929862897288,22.7579917088256,-42.6399262684548));
#21609=CARTESIAN_POINT('Ctrl Pts',(-26.7623689865021,23.2481784002927,-42.668163738631));
#21610=CARTESIAN_POINT('Ctrl Pts',(-26.7729948114299,23.3990451833679,-42.6769881055619));
#21611=CARTESIAN_POINT('Ctrl Pts',(-26.7730031690222,23.5626459800112,-42.686929797715));
#21612=CARTESIAN_POINT('Ctrl Pts',(-26.7729304079758,23.5752038179512,-42.6876951967023));
#21613=CARTESIAN_POINT('Ctrl Pts',(-26.7727305631484,23.5923735461849,-42.6887449119696));
#21614=CARTESIAN_POINT('Ctrl Pts',(-26.7726669694687,23.5969861804832,-42.6890272351));
#21615=CARTESIAN_POINT('Ctrl Pts',(-26.7725418143981,23.6048405690312,-42.6895085216415));
#21616=CARTESIAN_POINT('Ctrl Pts',(-26.7724852639444,23.608082405886,-42.6897073275621));
#21617=CARTESIAN_POINT('Ctrl Pts',(-26.7723663613252,23.6143557724717,-42.6900923515634));
#21618=CARTESIAN_POINT('Ctrl Pts',(-26.7723046228136,23.6173873109976,-42.6902785501383));
#21619=CARTESIAN_POINT('Ctrl Pts',(-26.7721478602195,23.6245857450682,-42.6907210154545));
#21620=CARTESIAN_POINT('Ctrl Pts',(-26.7720490308998,23.6287525446252,-42.6909774014118));
#21621=CARTESIAN_POINT('Ctrl Pts',(-26.7717332217499,23.6410602859584,-42.6917354965202));
#21622=CARTESIAN_POINT('Ctrl Pts',(-26.7714934679459,23.6492005650299,-42.6922379200724));
#21623=CARTESIAN_POINT('Ctrl Pts',(-26.7693729358582,23.7129819256551,-42.6961826877747));
#21624=CARTESIAN_POINT('Ctrl Pts',(-26.7660816035998,23.7685637455731,-42.6996691237189));
#21625=CARTESIAN_POINT('Ctrl Pts',(-26.749929619662,23.9580084090001,-42.7117297819845));
#21626=CARTESIAN_POINT('Ctrl Pts',(-26.7301343182387,24.0911243350592,-42.7205154458314));
#21627=CARTESIAN_POINT('Ctrl Pts',(-26.6373933776506,24.5258748386025,-42.7501456410641));
#21628=CARTESIAN_POINT('Ctrl Pts',(-26.5292722417456,24.8182113858969,-42.7717503436998));
#21629=CARTESIAN_POINT('Ctrl Pts',(-26.3737817774825,25.103968056285,-42.7923333706462));
#21630=CARTESIAN_POINT('Ctrl Pts',(-26.3664104822633,25.1172891465686,-42.7932911428775));
#21631=CARTESIAN_POINT('Ctrl Pts',(-26.3570222227504,25.1339749940236,-42.794488153266));
#21632=CARTESIAN_POINT('Ctrl Pts',(-26.3550933037446,25.1373886884717,-42.7947329029303));
#21633=CARTESIAN_POINT('Ctrl Pts',(-26.3519726255543,25.1428880355719,-42.7951269462766));
#21634=CARTESIAN_POINT('Ctrl Pts',(-26.3507847637066,25.1449758776391,-42.7952764899572));
#21635=CARTESIAN_POINT('Ctrl Pts',(-26.3486634220908,25.1486947679565,-42.7955427565334));
#21636=CARTESIAN_POINT('Ctrl Pts',(-26.3477308500097,25.1503263277374,-42.795659538285));
#21637=CARTESIAN_POINT('Ctrl Pts',(-26.345765351748,25.153758048638,-42.7959050944951));
#21638=CARTESIAN_POINT('Ctrl Pts',(-26.3447321161026,25.1555580235983,-42.7960338480734));
#21639=CARTESIAN_POINT('Ctrl Pts',(-26.3419960725353,25.1603137730059,-42.7963739192489));
#21640=CARTESIAN_POINT('Ctrl Pts',(-26.3402903034429,25.1632678543349,-42.7965850441716));
#21641=CARTESIAN_POINT('Ctrl Pts',(-26.3325400871556,25.1766407410522,-42.7975402998714));
#21642=CARTESIAN_POINT('Ctrl Pts',(-26.3264418450237,25.1870284956511,-42.7982809719925));
#21643=CARTESIAN_POINT('Ctrl Pts',(-26.1816643495727,25.4305056634149,-42.8156155831094));
#21644=CARTESIAN_POINT('Ctrl Pts',(-26.0141419164698,25.6452428918902,-42.8304032814843));
#21645=CARTESIAN_POINT('Ctrl Pts',(-25.7149858650322,25.9424607360275,-42.8540382761423));
#21646=CARTESIAN_POINT('Ctrl Pts',(-25.6010294874988,26.0408424941152,-42.8625526899209));
#21647=CARTESIAN_POINT('Ctrl Pts',(-25.4691774011028,26.1394704584868,-42.87221390628));
#21648=CARTESIAN_POINT('Ctrl Pts',(-25.4576676665194,26.1479610645109,-42.8730556642666));
#21649=CARTESIAN_POINT('Ctrl Pts',(-25.4405888475054,26.1603852206541,-42.8743026268573));
#21650=CARTESIAN_POINT('Ctrl Pts',(-25.4350630948944,26.1643782327105,-42.8747057545563));
#21651=CARTESIAN_POINT('Ctrl Pts',(-25.4262668707534,26.1706921597827,-42.8753469991283));
#21652=CARTESIAN_POINT('Ctrl Pts',(-25.4230046468484,26.173024569023,-42.8755847112169));
#21653=CARTESIAN_POINT('Ctrl Pts',(-25.4156735084646,26.1782455000225,-42.8761186923344));
#21654=CARTESIAN_POINT('Ctrl Pts',(-25.4116022276421,26.1811306685822,-42.8764150788139));
#21655=CARTESIAN_POINT('Ctrl Pts',(-25.4018615973445,26.1879995707798,-42.8771238362133));
#21656=CARTESIAN_POINT('Ctrl Pts',(-25.3961860845648,26.1919744874478,-42.8775365183289));
#21657=CARTESIAN_POINT('Ctrl Pts',(-25.3888365929864,26.197086547447,-42.8780705746595));
#21658=CARTESIAN_POINT('Ctrl Pts',(-25.3871742721678,26.1982404804455,-42.8781913456986));
#21659=CARTESIAN_POINT('Ctrl Pts',(-25.3815445806098,26.2021405903462,-42.8786002788691));
#21660=CARTESIAN_POINT('Ctrl Pts',(-25.3775721428924,26.2048794136122,-42.878888704554));
#21661=CARTESIAN_POINT('Ctrl Pts',(-25.3719468599377,26.2087391924316,-42.8792969667268));
#21662=CARTESIAN_POINT('Ctrl Pts',(-25.3702990875168,26.2098675574987,-42.8794165352257));
#21663=CARTESIAN_POINT('Ctrl Pts',(-25.3638707123897,26.2142608220175,-42.8798829228463));
#21664=CARTESIAN_POINT('Ctrl Pts',(-25.35908238543,26.2175143553336,-42.880230152109));
#21665=CARTESIAN_POINT('Ctrl Pts',(-25.3435836421814,26.2279843856537,-42.8813535349786));
#21666=CARTESIAN_POINT('Ctrl Pts',(-25.3328387034576,26.2351493428293,-42.8821315518111));
#21667=CARTESIAN_POINT('Ctrl Pts',(-25.3039186834693,26.2541837072214,-42.8842237045303));
#21668=CARTESIAN_POINT('Ctrl Pts',(-25.2856665019268,26.2659342306405,-42.8855421463071));
#21669=CARTESIAN_POINT('Ctrl Pts',(-25.2618743443805,26.2809135137602,-42.8872587441196));
#21670=CARTESIAN_POINT('Ctrl Pts',(-25.256441202096,26.2843115743443,-42.8876506081753));
#21671=CARTESIAN_POINT('Ctrl Pts',(-25.2477768349266,26.2896946616509,-42.8882753222793));
#21672=CARTESIAN_POINT('Ctrl Pts',(-25.2445521592834,26.2916902412186,-42.8885077821123));
#21673=CARTESIAN_POINT('Ctrl Pts',(-25.2387560977432,26.2952629814768,-42.8889255314625));
#21674=CARTESIAN_POINT('Ctrl Pts',(-25.2361860015664,26.2968422347697,-42.8891107435676));
#21675=CARTESIAN_POINT('Ctrl Pts',(-25.2301777337006,26.3005225391007,-42.8895436645211));
#21676=CARTESIAN_POINT('Ctrl Pts',(-25.2267378368535,26.3026207518507,-42.889791477387));
#21677=CARTESIAN_POINT('Ctrl Pts',(-25.2170224969143,26.3085217876392,-42.8904912536433));
#21678=CARTESIAN_POINT('Ctrl Pts',(-25.2107380178703,26.3123096190881,-42.8909437658583));
#21679=CARTESIAN_POINT('Ctrl Pts',(-25.1718189249581,26.335586413627,-42.8937452936679));
#21680=CARTESIAN_POINT('Ctrl Pts',(-25.1388557176521,26.3545175190888,-42.8961145495043));
#21681=CARTESIAN_POINT('Ctrl Pts',(-25.0404811514895,26.4087238895446,-42.9031784018418));
#21682=CARTESIAN_POINT('Ctrl Pts',(-24.9741795382192,26.442322772762,-42.9079310053756));
#21683=CARTESIAN_POINT('Ctrl Pts',(-24.7737068257992,26.5353486382798,-42.9222813716412));
#21684=CARTESIAN_POINT('Ctrl Pts',(-24.6365858724406,26.5879343773074,-42.9320801662562));
#21685=CARTESIAN_POINT('Ctrl Pts',(-24.3190657090242,26.6854474529186,-42.9545085646638));
#21686=CARTESIAN_POINT('Ctrl Pts',(-24.1373812674653,26.724493635316,-42.9671674935667));
#21687=CARTESIAN_POINT('Ctrl Pts',(-23.944443624342,26.7488164850273,-42.9799066384287));
#21688=CARTESIAN_POINT('Ctrl Pts',(-23.935541674287,26.749900990639,-42.9804928060862));
#21689=CARTESIAN_POINT('Ctrl Pts',(-23.9214534223858,26.7515576848575,-42.9814178267836));
#21690=CARTESIAN_POINT('Ctrl Pts',(-23.9162701145603,26.7521544531446,-42.9817575908504));
#21691=CARTESIAN_POINT('Ctrl Pts',(-23.9085947836463,26.7530192535508,-42.9822598460023));
#21692=CARTESIAN_POINT('Ctrl Pts',(-23.9061038837766,26.7532969677676,-42.9824227104421));
#21693=CARTESIAN_POINT('Ctrl Pts',(-23.8510150238207,26.7593738539185,-42.9860216288555));
#21694=CARTESIAN_POINT('Ctrl Pts',(-23.7982785290693,26.7638800237957,-42.9894065051399));
#21695=CARTESIAN_POINT('Ctrl Pts',(-23.7397115768795,26.7674338909795,-42.9930814223604));
#21696=CARTESIAN_POINT('Ctrl Pts',(-23.7339708694857,26.7677668210038,-42.993440740328));
#21697=CARTESIAN_POINT('Ctrl Pts',(-23.7259312181542,26.7682114902152,-42.9939426686887));
#21698=CARTESIAN_POINT('Ctrl Pts',(-23.7236330428516,26.7683361319187,-42.9940860006708));
#21699=CARTESIAN_POINT('Ctrl Pts',(-23.7194290760997,26.7685596178955,-42.9943479215933));
#21700=CARTESIAN_POINT('Ctrl Pts',(-23.7175233278509,26.7686592314575,-42.9944665541269));
#21701=CARTESIAN_POINT('Ctrl Pts',(-23.7136536332149,26.7688580541859,-42.9947072337291));
#21702=CARTESIAN_POINT('Ctrl Pts',(-23.7116896838639,26.7689571586119,-42.9948292747261));
#21703=CARTESIAN_POINT('Ctrl Pts',(-23.7068116924114,26.7691988350085,-42.9951321284785));
#21704=CARTESIAN_POINT('Ctrl Pts',(-23.7038975376462,26.7693392479435,-42.995312818822));
#21705=CARTESIAN_POINT('Ctrl Pts',(-23.6932050600677,26.7698398917377,-42.9959749423367));
#21706=CARTESIAN_POINT('Ctrl Pts',(-23.6854255479992,26.7701758930425,-42.9964550192184));
#21707=CARTESIAN_POINT('Ctrl Pts',(-23.4902013778715,26.7778989565271,-43.0084623570223));
#21708=CARTESIAN_POINT('Ctrl Pts',(-23.3024352674284,26.7689351101779,-43.0190948824889));
#21709=CARTESIAN_POINT('Ctrl Pts',(-22.8604541181004,26.7089009432671,-43.0440987794798));
#21710=CARTESIAN_POINT('Ctrl Pts',(-22.6095554302573,26.6434643067658,-43.0583441782979));
#21711=CARTESIAN_POINT('Ctrl Pts',(-22.3581892156027,26.5444538945471,-43.0743291516297));
#21712=CARTESIAN_POINT('Ctrl Pts',(-22.3472361732084,26.540069982122,-43.0750290372827));
#21713=CARTESIAN_POINT('Ctrl Pts',(-22.3299544988236,26.5330427201627,-43.0761387735316));
#21714=CARTESIAN_POINT('Ctrl Pts',(-22.3236097450076,26.530439114825,-43.0765473686224));
#21715=CARTESIAN_POINT('Ctrl Pts',(-22.3055903922116,26.5229774799171,-43.0777111710808));
#21716=CARTESIAN_POINT('Ctrl Pts',(-22.2939360981708,26.5180710017822,-43.0784679200922));
#21717=CARTESIAN_POINT('Ctrl Pts',(-22.2713968250993,26.5084253767869,-43.0799395096063));
#21718=CARTESIAN_POINT('Ctrl Pts',(-22.2605085518176,26.5036944153984,-43.080654072008));
#21719=CARTESIAN_POINT('Ctrl Pts',(-22.2452342047817,26.4969571296919,-43.0816617519892));
#21720=CARTESIAN_POINT('Ctrl Pts',(-22.2408260269479,26.4950009164835,-43.08195318887));
#21721=CARTESIAN_POINT('Ctrl Pts',(-22.218431093261,26.4850025073071,-43.0834369619699));
#21722=CARTESIAN_POINT('Ctrl Pts',(-22.2005142701219,26.4768055145826,-43.0846344956677));
#21723=CARTESIAN_POINT('Ctrl Pts',(-22.1770872020643,26.4658266788861,-43.0862144973648));
#21724=CARTESIAN_POINT('Ctrl Pts',(-22.171507926024,26.4631924455562,-43.0865918453896));
#21725=CARTESIAN_POINT('Ctrl Pts',(-22.162897531423,26.4590968020099,-43.0871758563069));
#21726=CARTESIAN_POINT('Ctrl Pts',(-22.159861058266,26.4576466288553,-43.0873821282361));
#21727=CARTESIAN_POINT('Ctrl Pts',(-22.1538113793065,26.4547457498651,-43.0877937310732));
#21728=CARTESIAN_POINT('Ctrl Pts',(-22.1507981491557,26.453295104159,-43.0879990596938));
#21729=CARTESIAN_POINT('Ctrl Pts',(-22.1441127285459,26.4500637449395,-43.0884553271919));
#21730=CARTESIAN_POINT('Ctrl Pts',(-22.1404416562234,26.4482807430166,-43.0887063457074));
#21731=CARTESIAN_POINT('Ctrl Pts',(-22.1299658720555,26.4431681470142,-43.089424015885));
#21732=CARTESIAN_POINT('Ctrl Pts',(-22.1231695339633,26.4398215426241,-43.0898912620281));
#21733=CARTESIAN_POINT('Ctrl Pts',(-22.1025516172965,26.4295785329546,-43.0913137850912));
#21734=CARTESIAN_POINT('Ctrl Pts',(-22.088768237422,26.4226069285476,-43.0922716814179));
#21735=CARTESIAN_POINT('Ctrl Pts',(-22.0750360145756,26.4155367741596,-43.0932330566435));
#21736=CARTESIAN_POINT('',(-26.7730012459478,23.5532182425584,-42.9355038191065));
#21737=CARTESIAN_POINT('Ctrl Pts',(-22.0750361136176,26.4155368251522,-43.341564988124));
#21738=CARTESIAN_POINT('Ctrl Pts',(-22.1509427032916,26.4546179898321,-43.3367652759782));
#21739=CARTESIAN_POINT('Ctrl Pts',(-22.2284014654945,26.4906823867973,-43.3320071409988));
#21740=CARTESIAN_POINT('Ctrl Pts',(-22.5314253727972,26.6173611431577,-43.3136374046661));
#21741=CARTESIAN_POINT('Ctrl Pts',(-22.7654593675607,26.6854142183436,-43.2998809977801));
#21742=CARTESIAN_POINT('Ctrl Pts',(-23.019686662624,26.729064029028,-43.2842307957217));
#21743=CARTESIAN_POINT('Ctrl Pts',(-23.0344914490408,26.7314996410399,-43.2833172542116));
#21744=CARTESIAN_POINT('Ctrl Pts',(-23.0547682160038,26.7346902147219,-43.2820629360421));
#21745=CARTESIAN_POINT('Ctrl Pts',(-23.0602260924065,26.7355346467322,-43.2817250036414));
#21746=CARTESIAN_POINT('Ctrl Pts',(-23.0688847564448,26.7368515173849,-43.2811883911328));
#21747=CARTESIAN_POINT('Ctrl Pts',(-23.0720841486359,26.737333175163,-43.2809900039576));
#21748=CARTESIAN_POINT('Ctrl Pts',(-23.0782857274384,26.7382572536265,-43.2806052467567));
#21749=CARTESIAN_POINT('Ctrl Pts',(-23.0812878255569,26.7387002536557,-43.2804188953232));
#21750=CARTESIAN_POINT('Ctrl Pts',(-23.0884317713322,26.7397441312741,-43.2799752139371));
#21751=CARTESIAN_POINT('Ctrl Pts',(-23.0925741648609,26.7403411810519,-43.2797177628843));
#21752=CARTESIAN_POINT('Ctrl Pts',(-23.1011546879221,26.7415608486552,-43.2791840954712));
#21753=CARTESIAN_POINT('Ctrl Pts',(-23.1055929744104,26.742182281074,-43.2789078420717));
#21754=CARTESIAN_POINT('Ctrl Pts',(-23.1308289876758,26.7456620781179,-43.2773358438323));
#21755=CARTESIAN_POINT('Ctrl Pts',(-23.1516525654624,26.7483263757426,-43.2760339657362));
#21756=CARTESIAN_POINT('Ctrl Pts',(-23.2842769950932,26.7639797533935,-43.2677107947191));
#21757=CARTESIAN_POINT('Ctrl Pts',(-23.3966554147684,26.771306482326,-43.2605115909895));
#21758=CARTESIAN_POINT('Ctrl Pts',(-23.6819401472285,26.7749429109132,-43.2418534081711));
#21759=CARTESIAN_POINT('Ctrl Pts',(-23.8545854562671,26.7632480547429,-43.230194448169));
#21760=CARTESIAN_POINT('Ctrl Pts',(-24.2245240346053,26.7080982289457,-43.204875831523));
#21761=CARTESIAN_POINT('Ctrl Pts',(-24.420411636503,26.6598303796107,-43.1912559840728));
#21762=CARTESIAN_POINT('Ctrl Pts',(-24.6222829617328,26.5894996631098,-43.1777724204905));
#21763=CARTESIAN_POINT('Ctrl Pts',(-24.6340088545185,26.5853381340295,-43.1769913630384));
#21764=CARTESIAN_POINT('Ctrl Pts',(-24.6491037292234,26.579882315304,-43.1759889466229));
#21765=CARTESIAN_POINT('Ctrl Pts',(-24.6524948389542,26.5786502064451,-43.1757639497925));
#21766=CARTESIAN_POINT('Ctrl Pts',(-24.6576760423978,26.5767578382635,-43.1754204944025));
#21767=CARTESIAN_POINT('Ctrl Pts',(-24.6594676164031,26.5761016850145,-43.1753017904183));
#21768=CARTESIAN_POINT('Ctrl Pts',(-24.6628330205577,26.5748657352924,-43.1750789183773));
#21769=CARTESIAN_POINT('Ctrl Pts',(-24.664406974584,26.5742863034969,-43.1749747290874));
#21770=CARTESIAN_POINT('Ctrl Pts',(-24.6680285047044,26.5729498705327,-43.1747351020247));
#21771=CARTESIAN_POINT('Ctrl Pts',(-24.670075760727,26.5721920188194,-43.1745997163465));
#21772=CARTESIAN_POINT('Ctrl Pts',(-24.6742756255496,26.5706324619997,-43.174322130593));
#21773=CARTESIAN_POINT('Ctrl Pts',(-24.6764281511334,26.5698305341925,-43.1741799439913));
#21774=CARTESIAN_POINT('Ctrl Pts',(-24.6868494873043,26.5659353506076,-43.1734919458912));
#21775=CARTESIAN_POINT('Ctrl Pts',(-24.6951065275419,26.5628103877854,-43.1729480226252));
#21776=CARTESIAN_POINT('Ctrl Pts',(-24.7158331253518,26.5548686681785,-43.1715854331672));
#21777=CARTESIAN_POINT('Ctrl Pts',(-24.7282858826642,26.5500081360755,-43.1707692883313));
#21778=CARTESIAN_POINT('Ctrl Pts',(-24.7781563947916,26.5301843454133,-43.1675095434055));
#21779=CARTESIAN_POINT('Ctrl Pts',(-24.8153239242216,26.5145966770975,-43.1650999266536));
#21780=CARTESIAN_POINT('Ctrl Pts',(-24.9438703527657,26.4578273417474,-43.1568030173911));
#21781=CARTESIAN_POINT('Ctrl Pts',(-25.0336183545985,26.4130816950656,-43.1510754175367));
#21782=CARTESIAN_POINT('Ctrl Pts',(-25.1941080437709,26.3234889160769,-43.1407025997512));
#21783=CARTESIAN_POINT('Ctrl Pts',(-25.2654644298278,26.2799319288187,-43.1360398852771));
#21784=CARTESIAN_POINT('Ctrl Pts',(-25.431619193957,26.1694181901096,-43.1248890819668));
#21785=CARTESIAN_POINT('Ctrl Pts',(-25.5246495743898,26.1000219310312,-43.1184006538264));
#21786=CARTESIAN_POINT('Ctrl Pts',(-25.6539676115307,25.9922279432827,-43.1087895065271));
#21787=CARTESIAN_POINT('Ctrl Pts',(-25.6933763416155,25.9577161424069,-43.1057743619891));
#21788=CARTESIAN_POINT('Ctrl Pts',(-25.8049385677268,25.8551059089662,-43.0969527498797));
#21789=CARTESIAN_POINT('Ctrl Pts',(-25.8748056359993,25.7846222454367,-43.0910638382995));
#21790=CARTESIAN_POINT('Ctrl Pts',(-25.9475815132422,25.7040907109088,-43.0844571203788));
#21791=CARTESIAN_POINT('Ctrl Pts',(-25.9538259928983,25.6971199616267,-43.0838862180708));
#21792=CARTESIAN_POINT('Ctrl Pts',(-25.9630464721434,25.6867364342051,-43.0830372006146));
#21793=CARTESIAN_POINT('Ctrl Pts',(-25.9660458234296,25.6833443806362,-43.0827600651662));
#21794=CARTESIAN_POINT('Ctrl Pts',(-25.9711653965373,25.6775298589418,-43.0822853785946));
#21795=CARTESIAN_POINT('Ctrl Pts',(-25.9732891616148,25.6751105072152,-43.0820879757709));
#21796=CARTESIAN_POINT('Ctrl Pts',(-25.9774116055984,25.6704000822708,-43.0817038453381));
#21797=CARTESIAN_POINT('Ctrl Pts',(-25.9794106747698,25.6681093545422,-43.0815171343298));
#21798=CARTESIAN_POINT('Ctrl Pts',(-25.9841807974182,25.6626276453863,-43.0810705610262));
#21799=CARTESIAN_POINT('Ctrl Pts',(-25.9869488160599,25.6594340414561,-43.0808105731081));
#21800=CARTESIAN_POINT('Ctrl Pts',(-25.9926762278723,25.6527997124927,-43.0802708523722));
#21801=CARTESIAN_POINT('Ctrl Pts',(-25.9956346494727,25.6493581643023,-43.0799910800869));
#21802=CARTESIAN_POINT('Ctrl Pts',(-26.0033471803171,25.6403477022209,-43.079259129514));
#21803=CARTESIAN_POINT('Ctrl Pts',(-26.0080895774494,25.6347688381916,-43.0788064692659));
#21804=CARTESIAN_POINT('Ctrl Pts',(-26.0487693912511,25.5865820724542,-43.074901130033));
#21805=CARTESIAN_POINT('Ctrl Pts',(-26.083612896262,25.5430669061555,-43.0714040691947));
#21806=CARTESIAN_POINT('Ctrl Pts',(-26.1995141587219,25.3903661971389,-43.0592221502688));
#21807=CARTESIAN_POINT('Ctrl Pts',(-26.2747728396409,25.2769796538916,-43.0503212471366));
#21808=CARTESIAN_POINT('Ctrl Pts',(-26.3664187966465,25.1179239288207,-43.0380682233437));
#21809=CARTESIAN_POINT('Ctrl Pts',(-26.3892787681611,25.0761345294865,-43.034870294632));
#21810=CARTESIAN_POINT('Ctrl Pts',(-26.4331633108364,24.9915083879703,-43.0284456893695));
#21811=CARTESIAN_POINT('Ctrl Pts',(-26.4541797551028,24.9486800747144,-43.025219737639));
#21812=CARTESIAN_POINT('Ctrl Pts',(-26.5501661064703,24.7415717359503,-43.0097696610343));
#21813=CARTESIAN_POINT('Ctrl Pts',(-26.6121976813115,24.5716367142189,-42.9975176262422));
#21814=CARTESIAN_POINT('Ctrl Pts',(-26.6603536598788,24.3948798423677,-42.9857021713235));
#21815=CARTESIAN_POINT('Ctrl Pts',(-26.6610340135151,24.3923706314408,-42.9855346300338));
#21816=CARTESIAN_POINT('Ctrl Pts',(-26.6719771648019,24.3518169898049,-42.9828299238098));
#21817=CARTESIAN_POINT('Ctrl Pts',(-26.6815449905338,24.3135861115317,-42.9803239013369));
#21818=CARTESIAN_POINT('Ctrl Pts',(-26.6914839806191,24.2705339725259,-42.9775580317215));
#21819=CARTESIAN_POINT('Ctrl Pts',(-26.6925479018824,24.2658782557377,-42.9772596598676));
#21820=CARTESIAN_POINT('Ctrl Pts',(-26.6941334151144,24.2588683425161,-42.9768115347045));
#21821=CARTESIAN_POINT('Ctrl Pts',(-26.6946627145101,24.2565159236234,-42.976661340515));
#21822=CARTESIAN_POINT('Ctrl Pts',(-26.6955743450391,24.252442932867,-42.9764016244539));
#21823=CARTESIAN_POINT('Ctrl Pts',(-26.6959579047328,24.2507226417437,-42.976292031464));
#21824=CARTESIAN_POINT('Ctrl Pts',(-26.69675363905,24.2471398845384,-42.9760640019667));
#21825=CARTESIAN_POINT('Ctrl Pts',(-26.6971655709079,24.2452773692289,-42.9759455800912));
#21826=CARTESIAN_POINT('Ctrl Pts',(-26.6981396317212,24.240854615942,-42.9756646577238));
#21827=CARTESIAN_POINT('Ctrl Pts',(-26.6987002928595,24.2382940483295,-42.9755022423958));
#21828=CARTESIAN_POINT('Ctrl Pts',(-26.6998762477183,24.2328918678211,-42.9751600554505));
#21829=CARTESIAN_POINT('Ctrl Pts',(-26.7004908218055,24.2300500982119,-42.9749803252388));
#21830=CARTESIAN_POINT('Ctrl Pts',(-26.7021530328351,24.2223134298431,-42.9744917493741));
#21831=CARTESIAN_POINT('Ctrl Pts',(-26.7031931177195,24.2174168905245,-42.9741833314858));
#21832=CARTESIAN_POINT('Ctrl Pts',(-26.7064013641297,24.2021379541389,-42.9732234018969));
#21833=CARTESIAN_POINT('Ctrl Pts',(-26.7085297099783,24.1917471371085,-42.9725740935284));
#21834=CARTESIAN_POINT('Ctrl Pts',(-26.7519035106713,23.9745422120992,-42.9590709954143));
#21835=CARTESIAN_POINT('Ctrl Pts',(-26.7728071020175,23.7641565808426,-42.9472921418563));
#21836=CARTESIAN_POINT('Ctrl Pts',(-26.7730011678017,23.5532174882307,-42.9355036403026));
#21837=CARTESIAN_POINT('Ctrl Pts',(-26.7730011671007,23.5532182500986,-42.9355036828802));
#21838=CARTESIAN_POINT('Ctrl Pts',(-26.7732206776241,23.3146833849243,-42.9221729691654));
#21839=CARTESIAN_POINT('Ctrl Pts',(-26.7469586553834,23.076880648849,-42.9088692482139));
#21840=CARTESIAN_POINT('Ctrl Pts',(-26.684120406286,22.7970455993921,-42.8917955242866));
#21841=CARTESIAN_POINT('Ctrl Pts',(-26.6724855231058,22.7501842192223,-42.8888899037176));
#21842=CARTESIAN_POINT('Ctrl Pts',(-26.6580400778509,22.6971293547783,-42.8855413888005));
#21843=CARTESIAN_POINT('Ctrl Pts',(-26.6562570795019,22.6906605732828,-42.8851321150198));
#21844=CARTESIAN_POINT('Ctrl Pts',(-26.6533035181252,22.6800741228125,-42.8844606599944));
#21845=CARTESIAN_POINT('Ctrl Pts',(-26.6521449238131,22.6759531120956,-42.8841988683537));
#21846=CARTESIAN_POINT('Ctrl Pts',(-26.6498768780253,22.6679471435574,-42.8836894723828));
#21847=CARTESIAN_POINT('Ctrl Pts',(-26.6487683243971,22.6640619379524,-42.8834418977168));
#21848=CARTESIAN_POINT('Ctrl Pts',(-26.6468190278943,22.6572785098653,-42.8830089898229));
#21849=CARTESIAN_POINT('Ctrl Pts',(-26.6459815130836,22.6543793583389,-42.8828237622843));
#21850=CARTESIAN_POINT('Ctrl Pts',(-26.6442185335528,22.648308599153,-42.8824354618323));
#21851=CARTESIAN_POINT('Ctrl Pts',(-26.6432922616326,22.6451372313043,-42.8822323626942));
#21852=CARTESIAN_POINT('Ctrl Pts',(-26.6407079219387,22.6363392692763,-42.8816682286616));
#21853=CARTESIAN_POINT('Ctrl Pts',(-26.6390393728553,22.6307157899285,-42.8813068508859));
#21854=CARTESIAN_POINT('Ctrl Pts',(-26.6323691989374,22.6084584382784,-42.8798733681443));
#21855=CARTESIAN_POINT('Ctrl Pts',(-26.6272485568308,22.5918608021945,-42.8787973651135));
#21856=CARTESIAN_POINT('Ctrl Pts',(-26.5403119610899,22.317951780387,-42.8609213293141));
#21857=CARTESIAN_POINT('Ctrl Pts',(-26.4266305769215,22.0719403799912,-42.8429861118193));
#21858=CARTESIAN_POINT('Ctrl Pts',(-26.2612559937834,21.8071614899485,-42.8218631250814));
#21859=CARTESIAN_POINT('Ctrl Pts',(-26.2381484476058,21.7717358178402,-42.8189987985425));
#21860=CARTESIAN_POINT('Ctrl Pts',(-26.1919273127832,21.7038344314972,-42.8134433823286));
#21861=CARTESIAN_POINT('Ctrl Pts',(-26.1688949303604,21.6713120022597,-42.8107523034702));
#21862=CARTESIAN_POINT('Ctrl Pts',(-26.0840253181362,21.5560663168118,-42.8011240275994));
#21863=CARTESIAN_POINT('Ctrl Pts',(-26.0188182410852,21.4758923672966,-42.7942493961707));
#21864=CARTESIAN_POINT('Ctrl Pts',(-25.9195477237839,21.365161906826,-42.7846402675818));
#21865=CARTESIAN_POINT('Ctrl Pts',(-25.8885135381685,21.3319836701529,-42.7817453708159));
#21866=CARTESIAN_POINT('Ctrl Pts',(-25.8543161380089,21.2969392000632,-42.7786811436662));
#21867=CARTESIAN_POINT('Ctrl Pts',(-25.8518417443447,21.2944118527135,-42.7784601198127));
#21868=CARTESIAN_POINT('Ctrl Pts',(-25.8477530346648,21.2902493722076,-42.7780960456291));
#21869=CARTESIAN_POINT('Ctrl Pts',(-25.8461411297105,21.288611891005,-42.7779528085938));
#21870=CARTESIAN_POINT('Ctrl Pts',(-25.8429940370427,21.2854216947814,-42.7776737253421));
#21871=CARTESIAN_POINT('Ctrl Pts',(-25.8414590203296,21.2838688138119,-42.7775378658036));
#21872=CARTESIAN_POINT('Ctrl Pts',(-25.8387421032135,21.2811258590118,-42.7772978705684));
#21873=CARTESIAN_POINT('Ctrl Pts',(-25.8375608581509,21.2799351540174,-42.7771936839051));
#21874=CARTESIAN_POINT('Ctrl Pts',(-25.8350341483264,21.2773921827844,-42.7769711614507));
#21875=CARTESIAN_POINT('Ctrl Pts',(-25.8336884162037,21.2760401927231,-42.7768528479161));
#21876=CARTESIAN_POINT('Ctrl Pts',(-25.8297951966268,21.2721358082554,-42.7765111472974));
#21877=CARTESIAN_POINT('Ctrl Pts',(-25.8272446140629,21.2695864833671,-42.7762880062305));
#21878=CARTESIAN_POINT('Ctrl Pts',(-25.8158864839073,21.2582720000677,-42.7752974855546));
#21879=CARTESIAN_POINT('Ctrl Pts',(-25.8070324118643,21.2495533885912,-42.7745337646571));
#21880=CARTESIAN_POINT('Ctrl Pts',(-25.6544360638322,21.1010201942704,-42.7615101847948));
#21881=CARTESIAN_POINT('Ctrl Pts',(-25.4979786022824,20.9748463711242,-42.750240755244));
#21882=CARTESIAN_POINT('Ctrl Pts',(-25.2332578675626,20.7993798523723,-42.7324765783569));
#21883=CARTESIAN_POINT('Ctrl Pts',(-25.1322857510813,20.7400963744484,-42.725965492665));
#21884=CARTESIAN_POINT('Ctrl Pts',(-24.9114308274586,20.6261094757991,-42.71190530181));
#21885=CARTESIAN_POINT('Ctrl Pts',(-24.7909734846356,20.5730012596527,-42.7043391769411));
#21886=CARTESIAN_POINT('Ctrl Pts',(-24.6161511215678,20.5083800237233,-42.6932646385291));
#21887=CARTESIAN_POINT('Ctrl Pts',(-24.5642107892402,20.4906747416888,-42.6899641633517));
#21888=CARTESIAN_POINT('Ctrl Pts',(-24.5063626728252,20.4725904373069,-42.6862689599717));
#21889=CARTESIAN_POINT('Ctrl Pts',(-24.5008746828447,20.4708908942324,-42.6859182121876));
#21890=CARTESIAN_POINT('Ctrl Pts',(-24.4905118985441,20.4677120473752,-42.6852555405896));
#21891=CARTESIAN_POINT('Ctrl Pts',(-24.4856380783167,20.466229608123,-42.6849437205553));
#21892=CARTESIAN_POINT('Ctrl Pts',(-24.4774068247731,20.4637472666001,-42.6844168318767));
#21893=CARTESIAN_POINT('Ctrl Pts',(-24.4740512274464,20.4627412678766,-42.6842019634287));
#21894=CARTESIAN_POINT('Ctrl Pts',(-24.4674098343044,20.4607619930267,-42.6837765467458));
#21895=CARTESIAN_POINT('Ctrl Pts',(-24.4641241127102,20.4597884824765,-42.6835660065137));
#21896=CARTESIAN_POINT('Ctrl Pts',(-24.4568812580183,20.4576550927498,-42.6831017419829));
#21897=CARTESIAN_POINT('Ctrl Pts',(-24.4529234430589,20.4564975652672,-42.6828479410905));
#21898=CARTESIAN_POINT('Ctrl Pts',(-24.4391056344832,20.4524850945711,-42.6819614751238));
#21899=CARTESIAN_POINT('Ctrl Pts',(-24.4292343099713,20.4496696893271,-42.6813275202032));
#21900=CARTESIAN_POINT('Ctrl Pts',(-24.3285911623559,20.4214844522414,-42.6748568998874));
#21901=CARTESIAN_POINT('Ctrl Pts',(-24.2367699056705,20.4000633930816,-42.6688924297269));
#21902=CARTESIAN_POINT('Ctrl Pts',(-24.0877672710488,20.3721263306123,-42.6591018476719));
#21903=CARTESIAN_POINT('Ctrl Pts',(-24.0311158018936,20.3630628346784,-42.6553543966523));
#21904=CARTESIAN_POINT('Ctrl Pts',(-23.8590258064222,20.3402232013328,-42.6439030095324));
#21905=CARTESIAN_POINT('Ctrl Pts',(-23.743060690231,20.3311764155558,-42.6360912314604));
#21906=CARTESIAN_POINT('Ctrl Pts',(-23.469509084614,20.324671379708,-42.6175908269821));
#21907=CARTESIAN_POINT('Ctrl Pts',(-23.3120820798332,20.3324625932331,-42.606882461056));
#21908=CARTESIAN_POINT('Ctrl Pts',(-23.0718318341764,20.3620873026283,-42.5909171521204));
#21909=CARTESIAN_POINT('Ctrl Pts',(-22.9882455603358,20.375754921397,-42.5854368989521));
#21910=CARTESIAN_POINT('Ctrl Pts',(-22.8999458416692,20.3937911452664,-42.5797940930526));
#21911=CARTESIAN_POINT('Ctrl Pts',(-22.8946079193113,20.3948955917597,-42.5794535495129));
#21912=CARTESIAN_POINT('Ctrl Pts',(-22.8873347536634,20.3964197043327,-42.5789903545931));
#21913=CARTESIAN_POINT('Ctrl Pts',(-22.885397097424,20.3968276102883,-42.5788670326369));
#21914=CARTESIAN_POINT('Ctrl Pts',(-22.8815384804972,20.3976436221017,-42.5786216095497));
#21915=CARTESIAN_POINT('Ctrl Pts',(-22.8796175144712,20.398051698493,-42.5784995067757));
#21916=CARTESIAN_POINT('Ctrl Pts',(-22.8758284117761,20.3988602490264,-42.5782588151013));
#21917=CARTESIAN_POINT('Ctrl Pts',(-22.8739602578487,20.3992606286329,-42.5781402209454));
#21918=CARTESIAN_POINT('Ctrl Pts',(-22.8698344318877,20.4001487069191,-42.5778784684429));
#21919=CARTESIAN_POINT('Ctrl Pts',(-22.8675769220889,20.4006371727122,-42.5777353544868));
#21920=CARTESIAN_POINT('Ctrl Pts',(-22.8598738026146,20.4023125963778,-42.5772473808399));
#21921=CARTESIAN_POINT('Ctrl Pts',(-22.8544307078257,20.4035112623084,-42.5769031929591));
#21922=CARTESIAN_POINT('Ctrl Pts',(-22.8007619685356,20.4154761319894,-42.573515373625));
#21923=CARTESIAN_POINT('Ctrl Pts',(-22.7527836248303,20.4273367178229,-42.5705334773686));
#21924=CARTESIAN_POINT('Ctrl Pts',(-22.700620908369,20.4415124086974,-42.567323937469));
#21925=CARTESIAN_POINT('Ctrl Pts',(-22.6961505304403,20.442737637185,-42.5670491403152));
#21926=CARTESIAN_POINT('Ctrl Pts',(-22.6885457086712,20.4448395951023,-42.5665820896246));
#21927=CARTESIAN_POINT('Ctrl Pts',(-22.6854099335051,20.4457114325768,-42.5663896283113));
#21928=CARTESIAN_POINT('Ctrl Pts',(-22.6771142218807,20.4480314279735,-42.5658807822747));
#21929=CARTESIAN_POINT('Ctrl Pts',(-22.6719565490922,20.4494877144195,-42.5655647379029));
#21930=CARTESIAN_POINT('Ctrl Pts',(-22.5463802065858,20.4852830806667,-42.5578771048344));
#21931=CARTESIAN_POINT('Ctrl Pts',(-22.4280503090522,20.5266016275272,-42.5507930199896));
#21932=CARTESIAN_POINT('Ctrl Pts',(-22.1639468031365,20.6364693975172,-42.5347513626917));
#21933=CARTESIAN_POINT('Ctrl Pts',(-22.0203114438457,20.7092571453548,-42.5258485516385));
#21934=CARTESIAN_POINT('Ctrl Pts',(-21.784945288413,20.8515750104061,-42.5101915519607));
#21935=CARTESIAN_POINT('Ctrl Pts',(-21.690401976134,20.9158413788921,-42.5035760120963));
#21936=CARTESIAN_POINT('Ctrl Pts',(-21.5730955054729,21.0050480150739,-42.4948000201833));
#21937=CARTESIAN_POINT('Ctrl Pts',(-21.5470269147369,21.025514338664,-42.4928115779633));
#21938=CARTESIAN_POINT('Ctrl Pts',(-21.5052858286745,21.0593385428865,-42.4895622899014));
#21939=CARTESIAN_POINT('Ctrl Pts',(-21.4894172016046,21.0724512830528,-42.488311264693));
#21940=CARTESIAN_POINT('Ctrl Pts',(-21.4702677926775,21.0885862453312,-42.4867818801817));
#21941=CARTESIAN_POINT('Ctrl Pts',(-21.4668659922368,21.0914646297287,-42.4865094269757));
#21942=CARTESIAN_POINT('Ctrl Pts',(-21.4602948397567,21.0970481433587,-42.4859816480036));
#21943=CARTESIAN_POINT('Ctrl Pts',(-21.4571247410851,21.0997523833657,-42.4857263591457));
#21944=CARTESIAN_POINT('Ctrl Pts',(-21.4516568736177,21.1044350772573,-42.4852848594542));
#21945=CARTESIAN_POINT('Ctrl Pts',(-21.4493566305251,21.1064106446494,-42.4850987682156));
#21946=CARTESIAN_POINT('Ctrl Pts',(-21.4446018971717,21.110505928954,-42.4847133603286));
#21947=CARTESIAN_POINT('Ctrl Pts',(-21.4421478124377,21.112626109788,-42.4845140245361));
#21948=CARTESIAN_POINT('Ctrl Pts',(-21.4354939640871,21.1183921956698,-42.4839724319685));
#21949=CARTESIAN_POINT('Ctrl Pts',(-21.4313004453642,21.1220452612138,-42.4836298772822));
#21950=CARTESIAN_POINT('Ctrl Pts',(-21.4156372537136,21.1357612821073,-42.4823458006032));
#21951=CARTESIAN_POINT('Ctrl Pts',(-21.4042297787779,21.1458946734697,-42.4814013336977));
#21952=CARTESIAN_POINT('Ctrl Pts',(-21.2197080378602,21.3121667935714,-42.4659706429489));
#21953=CARTESIAN_POINT('Ctrl Pts',(-21.0640023915785,21.4865219398689,-42.4506571947122));
#21954=CARTESIAN_POINT('Ctrl Pts',(-20.8202759413773,21.8274735407479,-42.4224106028467));
#21955=CARTESIAN_POINT('Ctrl Pts',(-20.7253802154318,21.9879339366995,-42.4096938737346));
#21956=CARTESIAN_POINT('Ctrl Pts',(-20.6197384702381,22.2080249112809,-42.3935991930763));
#21957=CARTESIAN_POINT('Ctrl Pts',(-20.5960346960134,22.2610335680038,-42.3898206935629));
#21958=CARTESIAN_POINT('Ctrl Pts',(-20.5632978955307,22.3398946266288,-42.3843709213058));
#21959=CARTESIAN_POINT('Ctrl Pts',(-20.5531422519381,22.3652654643725,-42.3826432074838));
#21960=CARTESIAN_POINT('Ctrl Pts',(-20.5417313472854,22.3948577499956,-42.3806600929655));
#21961=CARTESIAN_POINT('Ctrl Pts',(-20.5401609101612,22.3989553289121,-42.3803862045866));
#21962=CARTESIAN_POINT('Ctrl Pts',(-20.5377771679084,22.4052131991109,-42.3799690145268));
#21963=CARTESIAN_POINT('Ctrl Pts',(-20.5369578142754,22.4073711569943,-42.3798253495786));
#21964=CARTESIAN_POINT('Ctrl Pts',(-20.5355436710302,22.4111077236578,-42.3795769352665));
#21965=CARTESIAN_POINT('Ctrl Pts',(-20.5349478035115,22.4126859162869,-42.379472120642));
#21966=CARTESIAN_POINT('Ctrl Pts',(-20.5337073360189,22.4159791951783,-42.3792536226877));
#21967=CARTESIAN_POINT('Ctrl Pts',(-20.533062961257,22.4176943585446,-42.3791399532259));
#21968=CARTESIAN_POINT('Ctrl Pts',(-20.5312859048332,22.4224367155131,-42.3788260070789));
#21969=CARTESIAN_POINT('Ctrl Pts',(-20.530156309988,22.4254650756905,-42.3786259169079));
#21970=CARTESIAN_POINT('Ctrl Pts',(-20.5257498663559,22.4373329192826,-42.3778432855927));
#21971=CARTESIAN_POINT('Ctrl Pts',(-20.5225072119643,22.4461851784877,-42.377262779662));
#21972=CARTESIAN_POINT('Ctrl Pts',(-20.4680769244173,22.5968200422595,-42.3674378399944));
#21973=CARTESIAN_POINT('Ctrl Pts',(-20.4268522834777,22.7420297008173,-42.3587636207706));
#21974=CARTESIAN_POINT('Ctrl Pts',(-20.3561252584886,23.0797241947437,-42.3392808543728));
#21975=CARTESIAN_POINT('Ctrl Pts',(-20.3335767316978,23.27304527895,-42.3286004926776));
#21976=CARTESIAN_POINT('Ctrl Pts',(-20.3266567460818,23.5415475013397,-42.3133036561125));
#21977=CARTESIAN_POINT('Ctrl Pts',(-20.3273139357936,23.6159136226975,-42.3090215667337));
#21978=CARTESIAN_POINT('Ctrl Pts',(-20.3342510288998,23.7755267159733,-42.2996677505248));
#21979=CARTESIAN_POINT('Ctrl Pts',(-20.3413511576586,23.8606781944279,-42.2945769069961));
#21980=CARTESIAN_POINT('Ctrl Pts',(-20.3530421880274,23.9552984771299,-42.288772300936));
#21981=CARTESIAN_POINT('Ctrl Pts',(-20.3543055973687,23.965149373171,-42.2881662061302));
#21982=CARTESIAN_POINT('Ctrl Pts',(-20.3562168559389,23.9795246510271,-42.2872790909032));
#21983=CARTESIAN_POINT('Ctrl Pts',(-20.3568288360085,23.9840538109985,-42.2869992067027));
#21984=CARTESIAN_POINT('Ctrl Pts',(-20.3579133582044,23.9919535025763,-42.2865103605113));
#21985=CARTESIAN_POINT('Ctrl Pts',(-20.358381610301,23.9953246239407,-42.2863015347766));
#21986=CARTESIAN_POINT('Ctrl Pts',(-20.3592964105011,24.0018349150251,-42.285897833687));
#21987=CARTESIAN_POINT('Ctrl Pts',(-20.359742253156,24.004974181428,-42.2857029809207));
#21988=CARTESIAN_POINT('Ctrl Pts',(-20.3608100592867,24.0124139307051,-42.2852407515276));
#21989=CARTESIAN_POINT('Ctrl Pts',(-20.3614360877227,24.0167138161565,-42.2849732461435));
#21990=CARTESIAN_POINT('Ctrl Pts',(-20.3636652413472,24.031810571916,-42.2840327886188));
#21991=CARTESIAN_POINT('Ctrl Pts',(-20.3653145074074,24.0426004593252,-42.2833583730647));
#21992=CARTESIAN_POINT('Ctrl Pts',(-20.3877457810092,24.1845202755145,-42.2744575736255));
#21993=CARTESIAN_POINT('Ctrl Pts',(-20.4165538904434,24.3142349241154,-42.2659744731459));
#21994=CARTESIAN_POINT('Ctrl Pts',(-20.5021913105235,24.6117178789863,-42.2456763070632));
#21995=CARTESIAN_POINT('Ctrl Pts',(-20.5650075577419,24.777317108335,-42.2337142487038));
#21996=CARTESIAN_POINT('Ctrl Pts',(-20.691989605443,25.0437219173645,-42.2137419564363));
#21997=CARTESIAN_POINT('Ctrl Pts',(-20.7487469394587,25.1476526813279,-42.2057543563908));
#21998=CARTESIAN_POINT('Ctrl Pts',(-20.8402470588704,25.2952595329839,-42.1943199097766));
#21999=CARTESIAN_POINT('Ctrl Pts',(-20.8706077820063,25.3415324951484,-42.190722158966));
#22000=CARTESIAN_POINT('Ctrl Pts',(-20.9176157539124,25.4093054683775,-42.1854585774973));
#22001=CARTESIAN_POINT('Ctrl Pts',(-20.9333663566295,25.4314120388532,-42.1837426506835));
#22002=CARTESIAN_POINT('Ctrl Pts',(-20.9519822572153,25.4568537852271,-42.1817714958368));
#22003=CARTESIAN_POINT('Ctrl Pts',(-20.9545767462618,25.4603844582049,-42.1814980320123));
#22004=CARTESIAN_POINT('Ctrl Pts',(-20.9582862513728,25.465410970247,-42.1811088411842));
#22005=CARTESIAN_POINT('Ctrl Pts',(-20.959395363661,25.4669111288306,-42.1809927042112));
#22006=CARTESIAN_POINT('Ctrl Pts',(-20.9616336660534,25.4699331097948,-42.1807587883019));
#22007=CARTESIAN_POINT('Ctrl Pts',(-20.9627628981817,25.4714549026143,-42.1806410122555));
#22008=CARTESIAN_POINT('Ctrl Pts',(-20.9649563855117,25.4744054811903,-42.1804126944697));
#22009=CARTESIAN_POINT('Ctrl Pts',(-20.966020480369,25.4758343766084,-42.1803021418879));
#22010=CARTESIAN_POINT('Ctrl Pts',(-20.9685708172373,25.4792531164804,-42.1800376736622));
#22011=CARTESIAN_POINT('Ctrl Pts',(-20.9700581783799,25.4812421303427,-42.1798838369192));
#22012=CARTESIAN_POINT('Ctrl Pts',(-20.9754156266279,25.4883892808974,-42.1793311539395));
#22013=CARTESIAN_POINT('Ctrl Pts',(-20.9792989277195,25.493537563341,-42.1789332305905));
#22014=CARTESIAN_POINT('Ctrl Pts',(-21.0389497853282,25.5721278522812,-42.172861100148));
#22015=CARTESIAN_POINT('Ctrl Pts',(-21.0978351733072,25.6431629750485,-42.1674033130144));
#22016=CARTESIAN_POINT('Ctrl Pts',(-21.3038262492651,25.8710014843749,-42.1496313096764));
#22017=CARTESIAN_POINT('Ctrl Pts',(-21.46355327227,26.0156137231694,-42.1378685133145));
#22018=CARTESIAN_POINT('Ctrl Pts',(-21.7541545066487,26.2300907812917,-42.1175227770986));
#22019=CARTESIAN_POINT('Ctrl Pts',(-21.8775727270662,26.3088095223983,-42.1091568557875));
#22020=CARTESIAN_POINT('Ctrl Pts',(-22.028797831367,26.3913744481203,-42.098935492406));
#22021=CARTESIAN_POINT('Ctrl Pts',(-22.051844796427,26.4035965737945,-42.0973788457045));
#22022=CARTESIAN_POINT('Ctrl Pts',(-22.0750360182176,26.4155367760347,-42.0958126606468));
#22023=CARTESIAN_POINT('Origin',(-23.5502525316942,23.5502525316942,-77.3107734492734));
#22024=CARTESIAN_POINT('',(-22.0750360128358,26.4155367732638,-40.5991777786305));
#22025=CARTESIAN_POINT('',(-22.0750362323924,26.4155368863044,-40.843547806833));
#22026=CARTESIAN_POINT('',(-22.0750360153461,26.4155367745563,-77.3107734492734));
#22027=CARTESIAN_POINT('',(-26.7730012307853,23.547356844137,-41.4399333015911));
#22028=CARTESIAN_POINT('Ctrl Pts',(-22.0750360128358,26.4155367732638,-40.5991777786305));
#22029=CARTESIAN_POINT('Ctrl Pts',(-22.0432934995088,26.3991938641274,-40.6014730868289));
#22030=CARTESIAN_POINT('Ctrl Pts',(-22.0118213416415,26.3823228448258,-40.6037424340515));
#22031=CARTESIAN_POINT('Ctrl Pts',(-21.9754060074539,26.3620156445295,-40.6063549716233));
#22032=CARTESIAN_POINT('Ctrl Pts',(-21.9701872941625,26.3590863153357,-40.6067290547247));
#22033=CARTESIAN_POINT('Ctrl Pts',(-21.9628830495296,26.3549595524493,-40.6072521461456));
#22034=CARTESIAN_POINT('Ctrl Pts',(-21.9607906939689,26.3537743189625,-40.6074019336674));
#22035=CARTESIAN_POINT('Ctrl Pts',(-21.9571685747305,26.3517171787888,-40.6076611342999));
#22036=CARTESIAN_POINT('Ctrl Pts',(-21.9556381993199,26.3508463604878,-40.6077706178724));
#22037=CARTESIAN_POINT('Ctrl Pts',(-21.9524504024701,26.3490289717419,-40.6079986083742));
#22038=CARTESIAN_POINT('Ctrl Pts',(-21.9507931099509,26.3480821840737,-40.6081171004054));
#22039=CARTESIAN_POINT('Ctrl Pts',(-21.946901795441,26.3458545438681,-40.6083952339539));
#22040=CARTESIAN_POINT('Ctrl Pts',(-21.9446684593625,26.3445724812884,-40.6085547967429));
#22041=CARTESIAN_POINT('Ctrl Pts',(-21.937329762816,26.3403479470576,-40.6090789078208));
#22042=CARTESIAN_POINT('Ctrl Pts',(-21.9322308972587,26.3373941278454,-40.6094427228674));
#22043=CARTESIAN_POINT('Ctrl Pts',(-21.9202072363063,26.3303845964982,-40.610299918883));
#22044=CARTESIAN_POINT('Ctrl Pts',(-21.9132893938102,26.3263169493796,-40.6107925439051));
#22045=CARTESIAN_POINT('Ctrl Pts',(-21.7553460920893,26.2326516119365,-40.6220285633252));
#22046=CARTESIAN_POINT('Ctrl Pts',(-21.6118543082005,26.1308697745232,-40.632008045173));
#22047=CARTESIAN_POINT('Ctrl Pts',(-21.3263820560977,25.8910631721327,-40.6529301307129));
#22048=CARTESIAN_POINT('Ctrl Pts',(-21.1873727925544,25.7506594924681,-40.6638126096245));
#22049=CARTESIAN_POINT('Ctrl Pts',(-21.0245667138745,25.5528784006703,-40.678554441625));
#22050=CARTESIAN_POINT('Ctrl Pts',(-20.988326242029,25.5063027226929,-40.6819860439143));
#22051=CARTESIAN_POINT('Ctrl Pts',(-20.9115256726508,25.4018017980419,-40.6896300726272));
#22052=CARTESIAN_POINT('Ctrl Pts',(-20.8715533008564,25.343485196444,-40.6938605905363));
#22053=CARTESIAN_POINT('Ctrl Pts',(-20.8284201034018,25.275893315976,-40.6987441460454));
#22054=CARTESIAN_POINT('Ctrl Pts',(-20.8233431361462,25.2678593055246,-40.6993242875166));
#22055=CARTESIAN_POINT('Ctrl Pts',(-20.8159723810519,25.2560804550531,-40.7001744232374));
#22056=CARTESIAN_POINT('Ctrl Pts',(-20.8136505603031,25.2523531445203,-40.7004433793124));
#22057=CARTESIAN_POINT('Ctrl Pts',(-20.8095515198767,25.2457427254587,-40.7009202712371));
#22058=CARTESIAN_POINT('Ctrl Pts',(-20.8077712097385,25.2428615331809,-40.701128092626));
#22059=CARTESIAN_POINT('Ctrl Pts',(-20.804085531738,25.2368756787653,-40.7015597845266));
#22060=CARTESIAN_POINT('Ctrl Pts',(-20.8021808801656,25.2337705832088,-40.7017836810255));
#22061=CARTESIAN_POINT('Ctrl Pts',(-20.797288733894,25.2257646426548,-40.7023608624063));
#22062=CARTESIAN_POINT('Ctrl Pts',(-20.7943090691751,25.220859049307,-40.7027144343105));
#22063=CARTESIAN_POINT('Ctrl Pts',(-20.7821714944207,25.2007554192019,-40.7041630530388));
#22064=CARTESIAN_POINT('Ctrl Pts',(-20.7731262078621,25.1854900593326,-40.7052622108381));
#22065=CARTESIAN_POINT('Ctrl Pts',(-20.713828851719,25.0835052126581,-40.7126009486155));
#22066=CARTESIAN_POINT('Ctrl Pts',(-20.6675245785196,24.9945651867569,-40.7189820284134));
#22067=CARTESIAN_POINT('Ctrl Pts',(-20.5253943462227,24.6874025347923,-40.7409802985979));
#22068=CARTESIAN_POINT('Ctrl Pts',(-20.4496407799648,24.4607777254294,-40.7572121609062));
#22069=CARTESIAN_POINT('Ctrl Pts',(-20.366753221088,24.075405770627,-40.7837930126721));
#22070=CARTESIAN_POINT('Ctrl Pts',(-20.3450625654275,23.9206904125846,-40.7941831181307));
#22071=CARTESIAN_POINT('Ctrl Pts',(-20.3340398577299,23.755634133418,-40.8045864742499));
#22072=CARTESIAN_POINT('Ctrl Pts',(-20.3334556330648,23.746271114154,-40.8051742783703));
#22073=CARTESIAN_POINT('Ctrl Pts',(-20.3327255117376,23.7336860036915,-40.8059610999286));
#22074=CARTESIAN_POINT('Ctrl Pts',(-20.3325435630609,23.7304661721168,-40.8061621170052));
#22075=CARTESIAN_POINT('Ctrl Pts',(-20.3322659051648,23.7254181259619,-40.806476815705));
#22076=CARTESIAN_POINT('Ctrl Pts',(-20.3321669207041,23.7235901049899,-40.8065906821769));
#22077=CARTESIAN_POINT('Ctrl Pts',(-20.3319797042548,23.7200771979515,-40.806809318125));
#22078=CARTESIAN_POINT('Ctrl Pts',(-20.3318912383243,23.7183923379803,-40.8069141000011));
#22079=CARTESIAN_POINT('Ctrl Pts',(-20.3317113052865,23.7149132855507,-40.8071302981922));
#22080=CARTESIAN_POINT('Ctrl Pts',(-20.331620015588,23.7131190913317,-40.807241704033));
#22081=CARTESIAN_POINT('Ctrl Pts',(-20.3313451896625,23.7076272195437,-40.8075824332072));
#22082=CARTESIAN_POINT('Ctrl Pts',(-20.3311665239998,23.7039292845032,-40.8078114814788));
#22083=CARTESIAN_POINT('Ctrl Pts',(-20.3302808052685,23.6849175097961,-40.8089871421737));
#22084=CARTESIAN_POINT('Ctrl Pts',(-20.3296766390113,23.6695987373537,-40.8099280322875));
#22085=CARTESIAN_POINT('Ctrl Pts',(-20.3249943078711,23.5246109043877,-40.8187776517996));
#22086=CARTESIAN_POINT('Ctrl Pts',(-20.3286396827023,23.3947940002073,-40.8262821490169));
#22087=CARTESIAN_POINT('Ctrl Pts',(-20.3534906693657,23.1146020807431,-40.8422336692604));
#22088=CARTESIAN_POINT('Ctrl Pts',(-20.3775056893194,22.9647975980669,-40.8506125597583));
#22089=CARTESIAN_POINT('Ctrl Pts',(-20.4602008992774,22.6107528428476,-40.871034316267));
#22090=CARTESIAN_POINT('Ctrl Pts',(-20.5286806293075,22.4095678241394,-40.8831815796233));
#22091=CARTESIAN_POINT('Ctrl Pts',(-20.6218112809924,22.2046969659725,-40.8968526716497));
#22092=CARTESIAN_POINT('Ctrl Pts',(-20.6272850267819,22.1928473244589,-40.8976480583589));
#22093=CARTESIAN_POINT('Ctrl Pts',(-20.6348226021802,22.1767868886069,-40.8987325445493));
#22094=CARTESIAN_POINT('Ctrl Pts',(-20.6368239114543,22.1725467499551,-40.8990194759824));
#22095=CARTESIAN_POINT('Ctrl Pts',(-20.6402337323474,22.1653630782633,-40.8995066465937));
#22096=CARTESIAN_POINT('Ctrl Pts',(-20.6416374789106,22.1624172801676,-40.8997067199838));
#22097=CARTESIAN_POINT('Ctrl Pts',(-20.6443516741591,22.1567436774391,-40.9000926418929));
#22098=CARTESIAN_POINT('Ctrl Pts',(-20.6456614960899,22.1540155759809,-40.9002784684017));
#22099=CARTESIAN_POINT('Ctrl Pts',(-20.6487639845143,22.1475769616932,-40.9007176541141));
#22100=CARTESIAN_POINT('Ctrl Pts',(-20.6505599259456,22.1438680408772,-40.900971127359));
#22101=CARTESIAN_POINT('Ctrl Pts',(-20.6558275099628,22.1330425777109,-40.901712375135));
#22102=CARTESIAN_POINT('Ctrl Pts',(-20.6593182539854,22.1259354110119,-40.9022008168593));
#22103=CARTESIAN_POINT('Ctrl Pts',(-20.6840404118411,22.0760663141361,-40.9056408251687));
#22104=CARTESIAN_POINT('Ctrl Pts',(-20.7061926050644,22.0337698715937,-40.9086246244019));
#22105=CARTESIAN_POINT('Ctrl Pts',(-20.7578405964213,21.9402701303874,-40.9153749919312));
#22106=CARTESIAN_POINT('Ctrl Pts',(-20.7878209454303,21.8893555579867,-40.9191579589856));
#22107=CARTESIAN_POINT('Ctrl Pts',(-20.8888284125464,21.7281249654028,-40.931489341758));
#22108=CARTESIAN_POINT('Ctrl Pts',(-20.9651909657424,21.6213207478701,-40.9402122509415));
#22109=CARTESIAN_POINT('Ctrl Pts',(-21.1326803110029,21.4149331532857,-40.9581100519102));
#22110=CARTESIAN_POINT('Ctrl Pts',(-21.2239860436928,21.3158111584823,-40.9672733942923));
#22111=CARTESIAN_POINT('Ctrl Pts',(-21.4202667118616,21.127839614961,-40.9855284813944));
#22112=CARTESIAN_POINT('Ctrl Pts',(-21.5252778375254,21.0393938226189,-40.9945963623213));
#22113=CARTESIAN_POINT('Ctrl Pts',(-21.6420967466228,20.9531148916416,-41.0037170206215));
#22114=CARTESIAN_POINT('Ctrl Pts',(-21.6485929151767,20.9483545460506,-41.0042211975721));
#22115=CARTESIAN_POINT('Ctrl Pts',(-21.6573115271566,20.9420157048091,-41.0048937638975));
#22116=CARTESIAN_POINT('Ctrl Pts',(-21.6595181541871,20.9404156583198,-41.005063636589));
#22117=CARTESIAN_POINT('Ctrl Pts',(-21.6632244935742,20.9377353237225,-41.0053483715488));
#22118=CARTESIAN_POINT('Ctrl Pts',(-21.6647231048641,20.9366535266443,-41.0054633389914));
#22119=CARTESIAN_POINT('Ctrl Pts',(-21.6675884228123,20.9345888970782,-41.0056828449056));
#22120=CARTESIAN_POINT('Ctrl Pts',(-21.6689549605112,20.9336058522581,-41.0057873978757));
#22121=CARTESIAN_POINT('Ctrl Pts',(-21.6717741582797,20.931581158971,-41.0060028162599));
#22122=CARTESIAN_POINT('Ctrl Pts',(-21.6732269101469,20.9305396516636,-41.0061136717063));
#22123=CARTESIAN_POINT('Ctrl Pts',(-21.6764935752806,20.9282018253849,-41.0063626042634));
#22124=CARTESIAN_POINT('Ctrl Pts',(-21.6783079710218,20.9269061773141,-41.0065006347267));
#22125=CARTESIAN_POINT('Ctrl Pts',(-21.6866549663795,20.920958711831,-41.0071345683827));
#22126=CARTESIAN_POINT('Ctrl Pts',(-21.6932036465316,20.9163293517254,-41.0076289279773));
#22127=CARTESIAN_POINT('Ctrl Pts',(-21.7094523123623,20.9049336503199,-41.0088483269352));
#22128=CARTESIAN_POINT('Ctrl Pts',(-21.7191724810835,20.8981961051158,-41.0095714665436));
#22129=CARTESIAN_POINT('Ctrl Pts',(-21.7570645642291,20.8722388075072,-41.0123669477128));
#22130=CARTESIAN_POINT('Ctrl Pts',(-21.7855048503091,20.8534124509287,-41.0144149410903));
#22131=CARTESIAN_POINT('Ctrl Pts',(-21.9270681574466,20.7629017756342,-41.024392365917));
#22132=CARTESIAN_POINT('Ctrl Pts',(-22.0442948594015,20.6978587579274,-41.0319868114597));
#22133=CARTESIAN_POINT('Ctrl Pts',(-22.2485282882908,20.6006525408893,-41.0446815122091));
#22134=CARTESIAN_POINT('Ctrl Pts',(-22.3334811711318,20.5646045708852,-41.0498154962284));
#22135=CARTESIAN_POINT('Ctrl Pts',(-22.5228278512153,20.4936850121312,-41.061142067035));
#22136=CARTESIAN_POINT('Ctrl Pts',(-22.6276935862244,20.4604160595815,-41.0673422706006));
#22137=CARTESIAN_POINT('Ctrl Pts',(-22.7728182913045,20.4224226780869,-41.0759889501458));
#22138=CARTESIAN_POINT('Ctrl Pts',(-22.8117718617175,20.4129974067641,-41.0783158153718));
#22139=CARTESIAN_POINT('Ctrl Pts',(-22.8710408503275,20.3998215808066,-41.0818719534878));
#22140=CARTESIAN_POINT('Ctrl Pts',(-22.8912339039355,20.3955357288362,-41.083086269913));
#22141=CARTESIAN_POINT('Ctrl Pts',(-22.9160185410587,20.3905236862489,-41.0845806915805));
#22142=CARTESIAN_POINT('Ctrl Pts',(-22.9205726199284,20.3896129856492,-41.084855449926));
#22143=CARTESIAN_POINT('Ctrl Pts',(-22.9290637893124,20.3879340468324,-41.0853680587963));
#22144=CARTESIAN_POINT('Ctrl Pts',(-22.9330003802871,20.3871633083652,-41.0856058360436));
#22145=CARTESIAN_POINT('Ctrl Pts',(-22.9417757990838,20.3854621897809,-41.0861361773071));
#22146=CARTESIAN_POINT('Ctrl Pts',(-22.946615335699,20.3845355548271,-41.0864288503791));
#22147=CARTESIAN_POINT('Ctrl Pts',(-22.9582741827282,20.3823309207351,-41.0871344121659));
#22148=CARTESIAN_POINT('Ctrl Pts',(-22.9650955123168,20.3810638404964,-41.087547622131));
#22149=CARTESIAN_POINT('Ctrl Pts',(-22.9738272149612,20.3794710551626,-41.0880770907203));
#22150=CARTESIAN_POINT('Ctrl Pts',(-22.9757338979725,20.3791250260317,-41.0881927398401));
#22151=CARTESIAN_POINT('Ctrl Pts',(-22.9833472789303,20.3777504243222,-41.0886546582467));
#22152=CARTESIAN_POINT('Ctrl Pts',(-22.9890564116827,20.3767355392818,-41.0890013376986));
#22153=CARTESIAN_POINT('Ctrl Pts',(-22.9981313129363,20.3751475918589,-41.0895528833153));
#22154=CARTESIAN_POINT('Ctrl Pts',(-23.0014953241061,20.3745644572517,-41.0897574435849));
#22155=CARTESIAN_POINT('Ctrl Pts',(-23.0100394512387,20.3730973568166,-41.0902772715961));
#22156=CARTESIAN_POINT('Ctrl Pts',(-23.015220800795,20.3722207156186,-41.0905927615423));
#22157=CARTESIAN_POINT('Ctrl Pts',(-23.0360606025066,20.3687472034512,-41.0918627376422));
#22158=CARTESIAN_POINT('Ctrl Pts',(-23.0517358032043,20.3662533873181,-41.0928203672257));
#22159=CARTESIAN_POINT('Ctrl Pts',(-23.0851453848522,20.3611909147347,-41.094866861615));
#22160=CARTESIAN_POINT('Ctrl Pts',(-23.1028839891881,20.3586541826271,-41.0959566860303));
#22161=CARTESIAN_POINT('Ctrl Pts',(-23.1265296172773,20.3554737069772,-41.0974140391901));
#22162=CARTESIAN_POINT('Ctrl Pts',(-23.1324188296568,20.3546981441494,-41.0977773895984));
#22163=CARTESIAN_POINT('Ctrl Pts',(-23.1416015884516,20.3535146658704,-41.0983445472564));
#22164=CARTESIAN_POINT('Ctrl Pts',(-23.1448936987909,20.3530955457675,-41.0985479996766));
#22165=CARTESIAN_POINT('Ctrl Pts',(-23.1514787300525,20.3522675367062,-41.0989551984449));
#22166=CARTESIAN_POINT('Ctrl Pts',(-23.1547716468684,20.3518586468433,-41.0991589445056));
#22167=CARTESIAN_POINT('Ctrl Pts',(-23.1621847244827,20.3509497693323,-41.0996178983906));
#22168=CARTESIAN_POINT('Ctrl Pts',(-23.1663052256749,20.3504526544841,-41.0998731967094));
#22169=CARTESIAN_POINT('Ctrl Pts',(-23.1784297368068,20.3490136585173,-41.1006249802945));
#22170=CARTESIAN_POINT('Ctrl Pts',(-23.1864362891244,20.3480938451692,-41.101122162093));
#22171=CARTESIAN_POINT('Ctrl Pts',(-23.2446068067932,20.34163205049,-41.1047398002909));
#22172=CARTESIAN_POINT('Ctrl Pts',(-23.2948889632535,20.3372393536117,-41.107896345652));
#22173=CARTESIAN_POINT('Ctrl Pts',(-23.4427189776245,20.3278167082093,-41.1172701344927));
#22174=CARTESIAN_POINT('Ctrl Pts',(-23.5404096379684,20.3260385084828,-41.123585541634));
#22175=CARTESIAN_POINT('Ctrl Pts',(-23.6626933520622,20.3293700880169,-41.1316364464788));
#22176=CARTESIAN_POINT('Ctrl Pts',(-23.6873550095875,20.3303255879416,-41.1332674052219));
#22177=CARTESIAN_POINT('Ctrl Pts',(-23.8664357991741,20.3393250222433,-41.1451609414709));
#22178=CARTESIAN_POINT('Ctrl Pts',(-24.0201022950793,20.3581899973974,-41.1556524600215));
#22179=CARTESIAN_POINT('Ctrl Pts',(-24.3149287880935,20.4161398880161,-41.1759710422544));
#22180=CARTESIAN_POINT('Ctrl Pts',(-24.4559866552663,20.4539570795694,-41.1857763285285));
#22181=CARTESIAN_POINT('Ctrl Pts',(-24.6321169354082,20.5142503177353,-41.1977706164867));
#22182=CARTESIAN_POINT('Ctrl Pts',(-24.6699800972826,20.5280098901398,-41.2003333002545));
#22183=CARTESIAN_POINT('Ctrl Pts',(-24.7125584764869,20.5443930976456,-41.203189244162));
#22184=CARTESIAN_POINT('Ctrl Pts',(-24.7175347881309,20.5463220762172,-41.2035226257905));
#22185=CARTESIAN_POINT('Ctrl Pts',(-24.7247913243225,20.5491556981223,-41.2040081530552));
#22186=CARTESIAN_POINT('Ctrl Pts',(-24.7270753109588,20.5500505841307,-41.2041608831111));
#22187=CARTESIAN_POINT('Ctrl Pts',(-24.7311141466304,20.5516383570446,-41.2044307992432));
#22188=CARTESIAN_POINT('Ctrl Pts',(-24.7328694101176,20.5523301776327,-41.2045480500412));
#22189=CARTESIAN_POINT('Ctrl Pts',(-24.736530655884,20.5537769390663,-41.2047925062444));
#22190=CARTESIAN_POINT('Ctrl Pts',(-24.7384365216074,20.5545321556717,-41.2049196943245));
#22191=CARTESIAN_POINT('Ctrl Pts',(-24.7423008707186,20.5560677069925,-41.205177454823));
#22192=CARTESIAN_POINT('Ctrl Pts',(-24.7442593119227,20.55684814607,-41.2053080208203));
#22193=CARTESIAN_POINT('Ctrl Pts',(-24.7490805188733,20.5587748819318,-41.2056292826122));
#22194=CARTESIAN_POINT('Ctrl Pts',(-24.75194241521,20.5599233698937,-41.2058198464075));
#22195=CARTESIAN_POINT('Ctrl Pts',(-24.7784501493837,20.5706052062699,-41.207583654508));
#22196=CARTESIAN_POINT('Ctrl Pts',(-24.8019846062008,20.5804150809967,-41.2091403952101));
#22197=CARTESIAN_POINT('Ctrl Pts',(-24.873588747951,20.6112642902991,-41.213855759496));
#22198=CARTESIAN_POINT('Ctrl Pts',(-24.92126525473,20.6332000103845,-41.2169661361109));
#22199=CARTESIAN_POINT('Ctrl Pts',(-25.036262504893,20.6895524063899,-41.2244465007727));
#22200=CARTESIAN_POINT('Ctrl Pts',(-25.1029500358421,20.725192789201,-41.2287657648536));
#22201=CARTESIAN_POINT('Ctrl Pts',(-25.2281691915179,20.7978896349126,-41.2369524295764));
#22202=CARTESIAN_POINT('Ctrl Pts',(-25.2868792512434,20.8345511795097,-41.2408249536195));
#22203=CARTESIAN_POINT('Ctrl Pts',(-25.5756334268529,21.0280599426682,-41.2602532543347));
#22204=CARTESIAN_POINT('Ctrl Pts',(-25.7858094553284,21.2123298231566,-41.2757817689584));
#22205=CARTESIAN_POINT('Ctrl Pts',(-25.9816131934687,21.4348498025244,-41.2937314684605));
#22206=CARTESIAN_POINT('Ctrl Pts',(-25.9934229694182,21.4485005087917,-41.2948292194641));
#22207=CARTESIAN_POINT('Ctrl Pts',(-26.0089771620235,21.4667875697421,-41.2962956321584));
#22208=CARTESIAN_POINT('Ctrl Pts',(-26.0128244469236,21.4713363195683,-41.2966600494951));
#22209=CARTESIAN_POINT('Ctrl Pts',(-26.0187974555728,21.4784382160732,-41.2972284914128));
#22210=CARTESIAN_POINT('Ctrl Pts',(-26.0209318955351,21.4809840424506,-41.2974321584621));
#22211=CARTESIAN_POINT('Ctrl Pts',(-26.0251899574683,21.4860787726058,-41.2978395353777));
#22212=CARTESIAN_POINT('Ctrl Pts',(-26.0273135877231,21.4886276643185,-41.2980432445581));
#22213=CARTESIAN_POINT('Ctrl Pts',(-26.0320806555424,21.4943673463982,-41.2985017388625));
#22214=CARTESIAN_POINT('Ctrl Pts',(-26.0347218792043,21.4975599603456,-41.2987566137074));
#22215=CARTESIAN_POINT('Ctrl Pts',(-26.0424612955657,21.5069519020422,-41.2995059465733));
#22216=CARTESIAN_POINT('Ctrl Pts',(-26.0475424666117,21.5131651587655,-41.3000010942477));
#22217=CARTESIAN_POINT('Ctrl Pts',(-26.08419763603,21.5583303585132,-41.3035963584072));
#22218=CARTESIAN_POINT('Ctrl Pts',(-26.1148804741778,21.5979936363339,-41.3067320927743));
#22219=CARTESIAN_POINT('Ctrl Pts',(-26.238180436743,21.7653069448418,-41.319881982047));
#22220=CARTESIAN_POINT('Ctrl Pts',(-26.3222789106189,21.898936571663,-41.3302170095324));
#22221=CARTESIAN_POINT('Ctrl Pts',(-26.4213855392045,22.0854719062387,-41.3443570466273));
#22222=CARTESIAN_POINT('Ctrl Pts',(-26.4453349988727,22.1333953416888,-41.3479644217399));
#22223=CARTESIAN_POINT('Ctrl Pts',(-26.4792415960228,22.2056961515084,-41.3533586454581));
#22224=CARTESIAN_POINT('Ctrl Pts',(-26.4901129953055,22.229635539159,-41.355136993744));
#22225=CARTESIAN_POINT('Ctrl Pts',(-26.5126652040435,22.2809555970855,-41.358930676814));
#22226=CARTESIAN_POINT('Ctrl Pts',(-26.5242620986793,22.3083706348182,-41.3609461042242));
#22227=CARTESIAN_POINT('Ctrl Pts',(-26.606196915914,22.509796824941,-41.3756602322384));
#22228=CARTESIAN_POINT('Ctrl Pts',(-26.6616030779943,22.6895202703745,-41.3883030925025));
#22229=CARTESIAN_POINT('Ctrl Pts',(-26.703486323747,22.8843933240804,-41.4008652751921));
#22230=CARTESIAN_POINT('Ctrl Pts',(-26.7058600934959,22.8957353376166,-41.401592317885));
#22231=CARTESIAN_POINT('Ctrl Pts',(-26.7088730476672,22.9105289082338,-41.4025350517631));
#22232=CARTESIAN_POINT('Ctrl Pts',(-26.709567801794,22.9139688663901,-41.4027538752986));
#22233=CARTESIAN_POINT('Ctrl Pts',(-26.7106276855379,22.9192612369036,-41.4030899265937));
#22234=CARTESIAN_POINT('Ctrl Pts',(-26.7109968058331,22.9211128328391,-41.4032073835035));
#22235=CARTESIAN_POINT('Ctrl Pts',(-26.7117272735557,22.924793902693,-41.4034406650717));
#22236=CARTESIAN_POINT('Ctrl Pts',(-26.7120886581515,22.9266233554342,-41.4035564909728));
#22237=CARTESIAN_POINT('Ctrl Pts',(-26.7127941393426,22.9302111198549,-41.4037834186036));
#22238=CARTESIAN_POINT('Ctrl Pts',(-26.7131383559935,22.9319693967255,-41.4038945269232));
#22239=CARTESIAN_POINT('Ctrl Pts',(-26.7139104331432,22.9359307254931,-41.4041446184921));
#22240=CARTESIAN_POINT('Ctrl Pts',(-26.7143374596209,22.938133941945,-41.4042835537636));
#22241=CARTESIAN_POINT('Ctrl Pts',(-26.7154074560907,22.9436855591339,-41.4046332385633));
#22242=CARTESIAN_POINT('Ctrl Pts',(-26.7160474163126,22.9470345475399,-41.4048438167735));
#22243=CARTESIAN_POINT('Ctrl Pts',(-26.7178480845425,22.9565394542218,-41.4054404413024));
#22244=CARTESIAN_POINT('Ctrl Pts',(-26.7189961681716,22.9626977916105,-41.4058257803048));
#22245=CARTESIAN_POINT('Ctrl Pts',(-26.7551253405349,23.1596814307465,-41.4181135486117));
#22246=CARTESIAN_POINT('Ctrl Pts',(-26.7728268687897,23.3533010686489,-41.4290673617155));
#22247=CARTESIAN_POINT('Ctrl Pts',(-26.7730012307853,23.547356844137,-41.4399333015911));
#22248=CARTESIAN_POINT('Ctrl Pts',(-26.7730012290087,23.5473548674995,-41.4399331909115));
#22249=CARTESIAN_POINT('Ctrl Pts',(-26.7732549751028,23.8295683468469,-41.4557354257885));
#22250=CARTESIAN_POINT('Ctrl Pts',(-26.7364422799603,24.1105702441252,-41.471339060762));
#22251=CARTESIAN_POINT('Ctrl Pts',(-26.6577818407815,24.4045763104569,-41.4896146590668));
#22252=CARTESIAN_POINT('Ctrl Pts',(-26.6518408398425,24.4258994099139,-41.4909506825791));
#22253=CARTESIAN_POINT('Ctrl Pts',(-26.6428721030603,24.4568525529689,-41.4929061893761));
#22254=CARTESIAN_POINT('Ctrl Pts',(-26.6400179490036,24.4665325512064,-41.4935200412948));
#22255=CARTESIAN_POINT('Ctrl Pts',(-26.6348078181353,24.4839017809155,-41.4946257185757));
#22256=CARTESIAN_POINT('Ctrl Pts',(-26.6324684288685,24.4915959318628,-41.4951169992824));
#22257=CARTESIAN_POINT('Ctrl Pts',(-26.6288791446778,24.5032441036286,-41.4958630406758));
#22258=CARTESIAN_POINT('Ctrl Pts',(-26.6276503642386,24.5072046403937,-41.4961171073852));
#22259=CARTESIAN_POINT('Ctrl Pts',(-26.625510675283,24.514054425397,-41.4965572191203));
#22260=CARTESIAN_POINT('Ctrl Pts',(-26.6246033284534,24.5169447879887,-41.4967431467471));
#22261=CARTESIAN_POINT('Ctrl Pts',(-26.6227136850914,24.5229346974024,-41.4971289086737));
#22262=CARTESIAN_POINT('Ctrl Pts',(-26.6217307708624,24.5260340445379,-41.4973287631529));
#22263=CARTESIAN_POINT('Ctrl Pts',(-26.6193318806055,24.5335587410399,-41.4978145875779));
#22264=CARTESIAN_POINT('Ctrl Pts',(-26.6179110243099,24.5379825168535,-41.4981007182623));
#22265=CARTESIAN_POINT('Ctrl Pts',(-26.6125479623647,24.554556986721,-41.49917469805));
#22266=CARTESIAN_POINT('Ctrl Pts',(-26.6085431316802,24.5666871540768,-41.4999646134527));
#22267=CARTESIAN_POINT('Ctrl Pts',(-26.5421483128516,24.7638441625642,-41.5128682361771));
#22268=CARTESIAN_POINT('Ctrl Pts',(-26.4631539291189,24.9428132072715,-41.5255512014073));
#22269=CARTESIAN_POINT('Ctrl Pts',(-26.3160828759179,25.2079508373001,-41.5458227855924));
#22270=CARTESIAN_POINT('Ctrl Pts',(-26.2589837452152,25.2996966976019,-41.553135220738));
#22271=CARTESIAN_POINT('Ctrl Pts',(-26.1565857635696,25.4471611953628,-41.5652864392093));
#22272=CARTESIAN_POINT('Ctrl Pts',(-26.1138361829237,25.5045490000209,-41.5701229853691));
#22273=CARTESIAN_POINT('Ctrl Pts',(-26.0071713807481,25.6382084548427,-41.5815828848347));
#22274=CARTESIAN_POINT('Ctrl Pts',(-25.9415597577651,25.713043222035,-41.5881618092428));
#22275=CARTESIAN_POINT('Ctrl Pts',(-25.8496097342557,25.8086086047686,-41.5966613082357));
#22276=CARTESIAN_POINT('Ctrl Pts',(-25.8262655079964,25.8321335196531,-41.5987619659739));
#22277=CARTESIAN_POINT('Ctrl Pts',(-25.8002254147379,25.8575778783746,-41.6010390641041));
#22278=CARTESIAN_POINT('Ctrl Pts',(-25.7978858901472,25.8598569385266,-41.6012430697628));
#22279=CARTESIAN_POINT('Ctrl Pts',(-25.7939760841933,25.8636541295277,-41.601583037118));
#22280=CARTESIAN_POINT('Ctrl Pts',(-25.7924077236666,25.8651742210988,-41.6017191514159));
#22281=CARTESIAN_POINT('Ctrl Pts',(-25.7893262399283,25.8681547975615,-41.6019860768491));
#22282=CARTESIAN_POINT('Ctrl Pts',(-25.7878132304284,25.869615397776,-41.6021168970389));
#22283=CARTESIAN_POINT('Ctrl Pts',(-25.7849497936105,25.8723742380507,-41.6023640241589));
#22284=CARTESIAN_POINT('Ctrl Pts',(-25.7835996739742,25.8736727721236,-41.6024803540403));
#22285=CARTESIAN_POINT('Ctrl Pts',(-25.7805224250256,25.8766272845157,-41.6027450637949));
#22286=CARTESIAN_POINT('Ctrl Pts',(-25.7787945859516,25.8782825143536,-41.6028933846121));
#22287=CARTESIAN_POINT('Ctrl Pts',(-25.7736456030834,25.8832041355715,-41.6033344648278));
#22288=CARTESIAN_POINT('Ctrl Pts',(-25.7702190907472,25.8864649392672,-41.6036267885935));
#22289=CARTESIAN_POINT('Ctrl Pts',(-25.7464606709271,25.9089749160287,-41.605645470376));
#22290=CARTESIAN_POINT('Ctrl Pts',(-25.7258850395607,25.9279667273317,-41.6073522625333));
#22291=CARTESIAN_POINT('Ctrl Pts',(-25.7034145397294,25.9481715979209,-41.6091754439544));
#22292=CARTESIAN_POINT('Ctrl Pts',(-25.7017638686874,25.9496527583899,-41.6093091395614));
#22293=CARTESIAN_POINT('Ctrl Pts',(-25.5875956696382,26.0518842641419,-41.6185400889902));
#22294=CARTESIAN_POINT('Ctrl Pts',(-25.468121622834,26.1446152191126,-41.6271270845099));
#22295=CARTESIAN_POINT('Ctrl Pts',(-25.2762305005434,26.2730248805874,-41.6400936534042));
#22296=CARTESIAN_POINT('Ctrl Pts',(-25.2082642282798,26.3149381605884,-41.6445419841237));
#22297=CARTESIAN_POINT('Ctrl Pts',(-25.0692751545718,26.3936791691689,-41.6534764349294));
#22298=CARTESIAN_POINT('Ctrl Pts',(-24.998299079205,26.4304722107358,-41.6579594880579));
#22299=CARTESIAN_POINT('Ctrl Pts',(-24.816383035907,26.5163497905119,-41.6693805940293));
#22300=CARTESIAN_POINT('Ctrl Pts',(-24.7039118856048,26.5618775222612,-41.6763828192389));
#22301=CARTESIAN_POINT('Ctrl Pts',(-24.5397743009979,26.6177735203112,-41.6866990681911));
#22302=CARTESIAN_POINT('Ctrl Pts',(-24.4899991431198,26.6333863551346,-41.6898390555056));
#22303=CARTESIAN_POINT('Ctrl Pts',(-24.4321297177894,26.6500065590867,-41.6935101497815));
#22304=CARTESIAN_POINT('Ctrl Pts',(-24.4243820599904,26.6522003016602,-41.6940020578227));
#22305=CARTESIAN_POINT('Ctrl Pts',(-24.4126301106743,26.655480331304,-41.6947488598523));
#22306=CARTESIAN_POINT('Ctrl Pts',(-24.4086317691149,26.6565879708744,-41.6950030576987));
#22307=CARTESIAN_POINT('Ctrl Pts',(-24.4014319503373,26.6585675365645,-41.6954610030516));
#22308=CARTESIAN_POINT('Ctrl Pts',(-24.3982312390713,26.6594422467045,-41.6956646596145));
#22309=CARTESIAN_POINT('Ctrl Pts',(-24.3918258295243,26.6611821299848,-41.6960723785811));
#22310=CARTESIAN_POINT('Ctrl Pts',(-24.3886211339709,26.6620472980193,-41.6962764408736));
#22311=CARTESIAN_POINT('Ctrl Pts',(-24.3796743897362,26.664447816578,-41.6968463494232));
#22312=CARTESIAN_POINT('Ctrl Pts',(-24.3739294433942,26.6659722295112,-41.6972125505028));
#22313=CARTESIAN_POINT('Ctrl Pts',(-24.3508212870671,26.6720355660777,-41.6986865559263));
#22314=CARTESIAN_POINT('Ctrl Pts',(-24.3334247766313,26.6764452416261,-41.6997985418428));
#22315=CARTESIAN_POINT('Ctrl Pts',(-24.0469970420699,26.7465082433639,-41.7181473188033));
#22316=CARTESIAN_POINT('Ctrl Pts',(-23.7707023933676,26.7773471806951,-41.7365835982629));
#22317=CARTESIAN_POINT('Ctrl Pts',(-23.3586260498454,26.7701457734939,-41.7644782713857));
#22318=CARTESIAN_POINT('Ctrl Pts',(-23.2235886587777,26.7592597380725,-41.7736539242004));
#22319=CARTESIAN_POINT('Ctrl Pts',(-23.0072130592677,26.728012751157,-41.7880887461222));
#22320=CARTESIAN_POINT('Ctrl Pts',(-22.9252789790243,26.7129195640813,-41.7934896225253));
#22321=CARTESIAN_POINT('Ctrl Pts',(-22.8358922271599,26.6928432159545,-41.7992441421683));
#22322=CARTESIAN_POINT('Ctrl Pts',(-22.8277774302417,26.690987570651,-41.799765289005));
#22323=CARTESIAN_POINT('Ctrl Pts',(-22.8174737565613,26.6885893385273,-41.8004253194329));
#22324=CARTESIAN_POINT('Ctrl Pts',(-22.8152782343547,26.6880758901278,-41.8005658620517));
#22325=CARTESIAN_POINT('Ctrl Pts',(-22.8113361452357,26.687149622324,-41.8008180304982));
#22326=CARTESIAN_POINT('Ctrl Pts',(-22.8095893837548,26.6867376479829,-41.8009297050371));
#22327=CARTESIAN_POINT('Ctrl Pts',(-22.8062019441193,26.685935731491,-41.8011461490999));
#22328=CARTESIAN_POINT('Ctrl Pts',(-22.8045612294843,26.6855459610584,-41.8012509282751));
#22329=CARTESIAN_POINT('Ctrl Pts',(-22.8011367646558,26.6847296003248,-41.8014695037635));
#22330=CARTESIAN_POINT('Ctrl Pts',(-22.7993530776284,26.6843027763649,-41.8015832859783));
#22331=CARTESIAN_POINT('Ctrl Pts',(-22.7944177915531,26.6831173414367,-41.8018979290573));
#22332=CARTESIAN_POINT('Ctrl Pts',(-22.7912669600591,26.6823554950077,-41.8020986019821));
#22333=CARTESIAN_POINT('Ctrl Pts',(-22.7788941859147,26.6793440882427,-41.8028858259199));
#22334=CARTESIAN_POINT('Ctrl Pts',(-22.7696809310803,26.6770585136065,-41.8034703115351));
#22335=CARTESIAN_POINT('Ctrl Pts',(-22.6032394702727,26.634987104226,-41.814000524529));
#22336=CARTESIAN_POINT('Ctrl Pts',(-22.4492004563193,26.5834227235543,-41.8232859860548));
#22337=CARTESIAN_POINT('Ctrl Pts',(-22.223442254299,26.4883700572603,-41.8370777691865));
#22338=CARTESIAN_POINT('Ctrl Pts',(-22.1485068890778,26.4533639009463,-41.8416872496156));
#22339=CARTESIAN_POINT('Ctrl Pts',(-22.0750357700609,26.4155366482691,-41.8463063580885));
#22340=CARTESIAN_POINT('Ctrl Pts',(-22.0750360182176,26.4155367760347,-42.0958126606468));
#22341=CARTESIAN_POINT('Ctrl Pts',(-22.103435529259,26.4301585112938,-42.093894741434));
#22342=CARTESIAN_POINT('Ctrl Pts',(-22.1320513665457,26.4443574752129,-42.0919625094324));
#22343=CARTESIAN_POINT('Ctrl Pts',(-22.1683441668222,26.4616981131291,-42.0895105782871));
#22344=CARTESIAN_POINT('Ctrl Pts',(-22.1758278533202,26.4652384500172,-42.0890049140397));
#22345=CARTESIAN_POINT('Ctrl Pts',(-22.1871562798716,26.4705443097697,-42.0882393316427));
#22346=CARTESIAN_POINT('Ctrl Pts',(-22.1909910311223,26.4723311811528,-42.0879801536813));
#22347=CARTESIAN_POINT('Ctrl Pts',(-22.1975882309723,26.4753894686044,-42.0875342273135));
#22348=CARTESIAN_POINT('Ctrl Pts',(-22.2003489878723,26.4766645382981,-42.0873476055562));
#22349=CARTESIAN_POINT('Ctrl Pts',(-22.2060345469055,26.4792806853404,-42.0869632440204));
#22350=CARTESIAN_POINT('Ctrl Pts',(-22.2089595604265,26.480621293571,-42.086765488274));
#22351=CARTESIAN_POINT('Ctrl Pts',(-22.2159999928765,26.4838353533811,-42.0862894550494));
#22352=CARTESIAN_POINT('Ctrl Pts',(-22.2201173486565,26.4857045247541,-42.0860110303155));
#22353=CARTESIAN_POINT('Ctrl Pts',(-22.232745567747,26.4914053803569,-42.0851569726685));
#22354=CARTESIAN_POINT('Ctrl Pts',(-22.2412690976381,26.4952087360663,-42.0845803665874));
#22355=CARTESIAN_POINT('Ctrl Pts',(-22.3396071702622,26.538577726151,-42.0779259131648));
#22356=CARTESIAN_POINT('Ctrl Pts',(-22.4311585816821,26.5740539474951,-42.0717090230067));
#22357=CARTESIAN_POINT('Ctrl Pts',(-22.7526212868407,26.6820211974404,-42.0497727200448));
#22358=CARTESIAN_POINT('Ctrl Pts',(-22.9889241678932,26.7328724651795,-42.0333929910934));
#22359=CARTESIAN_POINT('Ctrl Pts',(-23.3956309345114,26.7736631907734,-42.0057942892784));
#22360=CARTESIAN_POINT('Ctrl Pts',(-23.5636999074674,26.7773439349881,-41.9945832226695));
#22361=CARTESIAN_POINT('Ctrl Pts',(-23.7388994679134,26.767485453607,-41.9835693633143));
#22362=CARTESIAN_POINT('Ctrl Pts',(-23.7464871964222,26.7670315572932,-41.9830937107103));
#22363=CARTESIAN_POINT('Ctrl Pts',(-23.7569246860861,26.7663701206404,-41.982441335042));
#22364=CARTESIAN_POINT('Ctrl Pts',(-23.7597758048045,26.7661856347775,-41.9822633284325));
#22365=CARTESIAN_POINT('Ctrl Pts',(-23.764588515374,26.7658677938415,-41.9819631891564));
#22366=CARTESIAN_POINT('Ctrl Pts',(-23.7665502304858,26.765736435184,-41.9818409436172));
#22367=CARTESIAN_POINT('Ctrl Pts',(-23.7704162493744,26.7654740082709,-41.9816002182953));
#22368=CARTESIAN_POINT('Ctrl Pts',(-23.7723205570652,26.765343043354,-41.9814817328617));
#22369=CARTESIAN_POINT('Ctrl Pts',(-23.7765221849072,26.7650503340997,-41.9812205054206));
#22370=CARTESIAN_POINT('Ctrl Pts',(-23.7788194542811,26.7648878186735,-41.9810778071544));
#22371=CARTESIAN_POINT('Ctrl Pts',(-23.7868604681311,26.7643103111411,-41.980578775518));
#22372=CARTESIAN_POINT('Ctrl Pts',(-23.7926033169498,26.7638823833276,-41.9802231696573));
#22373=CARTESIAN_POINT('Ctrl Pts',(-23.8513920459098,26.7593432620782,-41.9765907926088));
#22374=CARTESIAN_POINT('Ctrl Pts',(-23.9043333245994,26.7539341522394,-41.9733856488535));
#22375=CARTESIAN_POINT('Ctrl Pts',(-24.2452295993857,26.7105493527416,-41.953034396382));
#22376=CARTESIAN_POINT('Ctrl Pts',(-24.5270920610261,26.6351022259567,-41.9374305435732));
#22377=CARTESIAN_POINT('Ctrl Pts',(-24.9041715074109,26.4771989149843,-41.9141955019111));
#22378=CARTESIAN_POINT('Ctrl Pts',(-25.0106792040042,26.4255371264115,-41.9073561122829));
#22379=CARTESIAN_POINT('Ctrl Pts',(-25.1590189618754,26.3432128494596,-41.8972586203119));
#22380=CARTESIAN_POINT('Ctrl Pts',(-25.2033337081218,26.3172145711945,-41.8941653871063));
#22381=CARTESIAN_POINT('Ctrl Pts',(-25.2537744956299,26.2859780033777,-41.8905478244237));
#22382=CARTESIAN_POINT('Ctrl Pts',(-25.2605270684221,26.2817616283763,-41.8900615000232));
#22383=CARTESIAN_POINT('Ctrl Pts',(-25.2707875565535,26.275301912558,-41.8893193976525));
#22384=CARTESIAN_POINT('Ctrl Pts',(-25.2743068952844,26.2730766999138,-41.8890642926153));
#22385=CARTESIAN_POINT('Ctrl Pts',(-25.2803812692958,26.26921948726,-41.8886230007464));
#22386=CARTESIAN_POINT('Ctrl Pts',(-25.2829383383632,26.2675906868379,-41.8884369331774));
#22387=CARTESIAN_POINT('Ctrl Pts',(-25.2882270394536,26.2642113926472,-41.8880514696754));
#22388=CARTESIAN_POINT('Ctrl Pts',(-25.2909583332358,26.2624603778809,-41.8878520544404));
#22389=CARTESIAN_POINT('Ctrl Pts',(-25.2975726966992,26.2582058454247,-41.8873682876139));
#22390=CARTESIAN_POINT('Ctrl Pts',(-25.3014530280401,26.255698101213,-41.8870837781584));
#22391=CARTESIAN_POINT('Ctrl Pts',(-25.3158979355521,26.2463186845774,-41.8860220159166));
#22392=CARTESIAN_POINT('Ctrl Pts',(-25.3264274601538,26.2393934742905,-41.8852427567348));
#22393=CARTESIAN_POINT('Ctrl Pts',(-25.5051668519446,26.1203298000408,-41.8719233000398));
#22394=CARTESIAN_POINT('Ctrl Pts',(-25.6624657071992,25.9926928642343,-41.8587706239451));
#22395=CARTESIAN_POINT('Ctrl Pts',(-26.0176260912968,25.6443916279302,-41.8254602185934));
#22396=CARTESIAN_POINT('Ctrl Pts',(-26.199071050756,25.4095864743887,-41.8049573570652));
#22397=CARTESIAN_POINT('Ctrl Pts',(-26.3501372397187,25.1461323551671,-41.7858036819124));
#22398=CARTESIAN_POINT('Ctrl Pts',(-26.3542480852093,25.1388984106195,-41.785280593873));
#22399=CARTESIAN_POINT('Ctrl Pts',(-26.3613286502356,25.1263254803698,-41.7843764573285));
#22400=CARTESIAN_POINT('Ctrl Pts',(-26.3643112662188,25.1209938610937,-41.78399460873));
#22401=CARTESIAN_POINT('Ctrl Pts',(-26.3685518275275,25.113362736088,-41.7834503252597));
#22402=CARTESIAN_POINT('Ctrl Pts',(-26.3698221326855,25.1110701691067,-41.783287099844));
#22403=CARTESIAN_POINT('Ctrl Pts',(-26.3720120992346,25.1071064567436,-41.7830053968559));
#22404=CARTESIAN_POINT('Ctrl Pts',(-26.3729330749773,25.1054360422781,-41.7828868341231));
#22405=CARTESIAN_POINT('Ctrl Pts',(-26.3747022190419,25.1022205187516,-41.782658900918));
#22406=CARTESIAN_POINT('Ctrl Pts',(-26.3755506011701,25.1006755345753,-41.7825495164983));
#22407=CARTESIAN_POINT('Ctrl Pts',(-26.377556678072,25.0970151642473,-41.7822906743768));
#22408=CARTESIAN_POINT('Ctrl Pts',(-26.3787132688805,25.0948991695606,-41.7821412880803));
#22409=CARTESIAN_POINT('Ctrl Pts',(-26.3821537440466,25.0885879638409,-41.7816964516389));
#22410=CARTESIAN_POINT('Ctrl Pts',(-26.3844306906493,25.0843889475049,-41.7814014448405));
#22411=CARTESIAN_POINT('Ctrl Pts',(-26.4054171084777,25.0454807974827,-41.7786765895041));
#22412=CARTESIAN_POINT('Ctrl Pts',(-26.4234984646403,25.0104341920233,-41.7762860155738));
#22413=CARTESIAN_POINT('Ctrl Pts',(-26.5134741122263,24.8278899737184,-41.7641152868074));
#22414=CARTESIAN_POINT('Ctrl Pts',(-26.5746787837715,24.675373913756,-41.7548728277085));
#22415=CARTESIAN_POINT('Ctrl Pts',(-26.6734921586445,24.3617970430938,-41.7364715947313));
#22416=CARTESIAN_POINT('Ctrl Pts',(-26.7108705776233,24.2011912606758,-41.7273353721418));
#22417=CARTESIAN_POINT('Ctrl Pts',(-26.755251966279,23.9115902208762,-41.7105552290491));
#22418=CARTESIAN_POINT('Ctrl Pts',(-26.7670956244258,23.7837067609564,-41.7030451021251));
#22419=CARTESIAN_POINT('Ctrl Pts',(-26.7717319542035,23.6417713003537,-41.694456879179));
#22420=CARTESIAN_POINT('Ctrl Pts',(-26.7720919790689,23.6280723301105,-41.6936254608581));
#22421=CARTESIAN_POINT('Ctrl Pts',(-26.7725694938201,23.6040762696143,-41.6921644978409));
#22422=CARTESIAN_POINT('Ctrl Pts',(-26.7727250216825,23.5937800697245,-41.6915361491234));
#22423=CARTESIAN_POINT('Ctrl Pts',(-26.7728785049626,23.5788959558208,-41.6906256165344));
#22424=CARTESIAN_POINT('Ctrl Pts',(-26.7729160143181,23.5743084404711,-41.6903446747312));
#22425=CARTESIAN_POINT('Ctrl Pts',(-26.7729643056428,23.5663145403464,-41.6898545932175));
#22426=CARTESIAN_POINT('Ctrl Pts',(-26.7729794826565,23.5629081812731,-41.6896455917956));
#22427=CARTESIAN_POINT('Ctrl Pts',(-26.7729983462488,23.556335521612,-41.6892419914677));
#22428=CARTESIAN_POINT('Ctrl Pts',(-26.7730027672509,23.5531692255332,-41.689047415855));
#22429=CARTESIAN_POINT('Ctrl Pts',(-26.7730021219335,23.5448369336704,-41.6885349914323));
#22430=CARTESIAN_POINT('Ctrl Pts',(-26.7729893003427,23.5396709631253,-41.6882168994899));
#22431=CARTESIAN_POINT('Ctrl Pts',(-26.7728965858869,23.5206969884614,-41.687047132472));
#22432=CARTESIAN_POINT('Ctrl Pts',(-26.7727403721608,23.5068896597323,-41.6861930650199));
#22433=CARTESIAN_POINT('Ctrl Pts',(-26.7692984497465,23.3128896303722,-41.6741522272646));
#22434=CARTESIAN_POINT('Ctrl Pts',(-26.750993015845,23.1333135249129,-41.6624845816784));
#22435=CARTESIAN_POINT('Ctrl Pts',(-26.6603131905545,22.6497749137069,-41.6297077263732));
#22436=CARTESIAN_POINT('Ctrl Pts',(-26.558677767537,22.3532920686262,-41.6079762439181));
#22437=CARTESIAN_POINT('Ctrl Pts',(-26.408750229919,22.0618430067611,-41.587238713448));
#22438=CARTESIAN_POINT('Ctrl Pts',(-26.4013480512056,22.0477125594052,-41.5862354230954));
#22439=CARTESIAN_POINT('Ctrl Pts',(-26.3921631841033,22.0304913271692,-41.5850158436686));
#22440=CARTESIAN_POINT('Ctrl Pts',(-26.3904800577144,22.0273481105974,-41.5847933759045));
#22441=CARTESIAN_POINT('Ctrl Pts',(-26.3876937039386,22.022165317757,-41.5844267752399));
#22442=CARTESIAN_POINT('Ctrl Pts',(-26.3865934915174,22.0201241387003,-41.5842824511349));
#22443=CARTESIAN_POINT('Ctrl Pts',(-26.3846036755462,22.0164420349798,-41.5840222089095));
#22444=CARTESIAN_POINT('Ctrl Pts',(-26.3837148517011,22.0148006999372,-41.583906241351));
#22445=CARTESIAN_POINT('Ctrl Pts',(-26.3817981199284,22.011268523962,-41.5836567598176));
#22446=CARTESIAN_POINT('Ctrl Pts',(-26.3807697466107,22.0093779454833,-41.5835232766579));
#22447=CARTESIAN_POINT('Ctrl Pts',(-26.3779422157224,22.0041921484269,-41.5831572713244));
#22448=CARTESIAN_POINT('Ctrl Pts',(-26.3761391853438,22.0008990281535,-41.5829249976214));
#22449=CARTESIAN_POINT('Ctrl Pts',(-26.3666618003489,21.9836607674687,-41.5817098752807));
#22450=CARTESIAN_POINT('Ctrl Pts',(-26.3588897891211,21.9697691546514,-41.5807332129175));
#22451=CARTESIAN_POINT('Ctrl Pts',(-26.2607467820825,21.7973597658276,-41.5686365518939));
#22452=CARTESIAN_POINT('Ctrl Pts',(-26.1571593423471,21.646711271517,-41.5583192103698));
#22453=CARTESIAN_POINT('Ctrl Pts',(-25.9019960897186,21.3358287241443,-41.5357884006329));
#22454=CARTESIAN_POINT('Ctrl Pts',(-25.7456488990525,21.1807381398713,-41.5236472019806));
#22455=CARTESIAN_POINT('Ctrl Pts',(-25.5009540886434,20.9831771098063,-41.5053098041991));
#22456=CARTESIAN_POINT('Ctrl Pts',(-25.4245726722362,20.9268894038697,-41.4996724978878));
#22457=CARTESIAN_POINT('Ctrl Pts',(-25.3372882867543,20.8683266420224,-41.4932742181114));
#22458=CARTESIAN_POINT('Ctrl Pts',(-25.3287233313674,20.8626393008863,-41.4926468479523));
#22459=CARTESIAN_POINT('Ctrl Pts',(-25.3166830253648,20.8547269985375,-41.4917655211818));
#22460=CARTESIAN_POINT('Ctrl Pts',(-25.3132303292048,20.8524675376489,-41.4915128602624));
#22461=CARTESIAN_POINT('Ctrl Pts',(-25.3069016403312,20.8483433511008,-41.4910498634251));
#22462=CARTESIAN_POINT('Ctrl Pts',(-25.3040269896045,20.846476568029,-41.4908396048734));
#22463=CARTESIAN_POINT('Ctrl Pts',(-25.2982090228235,20.8427115931514,-41.4904141563898));
#22464=CARTESIAN_POINT('Ctrl Pts',(-25.2952655805354,20.8408136067531,-41.4901989592079));
#22465=CARTESIAN_POINT('Ctrl Pts',(-25.2880365735255,20.8361688746953,-41.4896705530323));
#22466=CARTESIAN_POINT('Ctrl Pts',(-25.2837475944094,20.8334274839043,-41.4893571450565));
#22467=CARTESIAN_POINT('Ctrl Pts',(-25.2684774740081,20.823718147515,-41.4882416407818));
#22468=CARTESIAN_POINT('Ctrl Pts',(-25.2574607822162,20.8168065962708,-41.4874374547109));
#22469=CARTESIAN_POINT('Ctrl Pts',(-25.1069945473078,20.7236729214604,-41.476461179445));
#22470=CARTESIAN_POINT('Ctrl Pts',(-24.9612283174509,20.6481618870958,-41.4658937522375));
#22471=CARTESIAN_POINT('Ctrl Pts',(-24.5360806544897,20.4675468710269,-41.4352680821289));
#22472=CARTESIAN_POINT('Ctrl Pts',(-24.2469792010347,20.3896372875369,-41.414548609095));
#22473=CARTESIAN_POINT('Ctrl Pts',(-23.945568945234,20.3518348135755,-41.3949246539071));
#22474=CARTESIAN_POINT('Ctrl Pts',(-23.9398322955239,20.3511309999318,-41.3945519317201));
#22475=CARTESIAN_POINT('Ctrl Pts',(-23.895416897762,20.3458030396867,-41.3916723187784));
#22476=CARTESIAN_POINT('Ctrl Pts',(-23.8566569034844,20.3418648233006,-41.3891954182124));
#22477=CARTESIAN_POINT('Ctrl Pts',(-23.8130892639357,20.3382349300513,-41.3864587722502));
#22478=CARTESIAN_POINT('Ctrl Pts',(-23.8083446908445,20.3378502126881,-41.3861613788571));
#22479=CARTESIAN_POINT('Ctrl Pts',(-23.8011994424737,20.3372867669619,-41.3857144769748));
#22480=CARTESIAN_POINT('Ctrl Pts',(-23.7987994173122,20.3371002161146,-41.3855645309411));
#22481=CARTESIAN_POINT('Ctrl Pts',(-23.7946428199316,20.3367818141671,-41.3853051269828));
#22482=CARTESIAN_POINT('Ctrl Pts',(-23.7928863489686,20.3366487141495,-41.3851955983429));
#22483=CARTESIAN_POINT('Ctrl Pts',(-23.7892267996733,20.3363744220945,-41.3849675852566));
#22484=CARTESIAN_POINT('Ctrl Pts',(-23.7873237070643,20.336233480421,-41.3848491156088));
#22485=CARTESIAN_POINT('Ctrl Pts',(-23.7828547191302,20.3359065012697,-41.3845711606338));
#22486=CARTESIAN_POINT('Ctrl Pts',(-23.7802887168432,20.3357218451805,-41.3844117537296));
#22487=CARTESIAN_POINT('Ctrl Pts',(-23.7718611315177,20.3351255173343,-41.3838888229272));
#22488=CARTESIAN_POINT('Ctrl Pts',(-23.765998599524,20.3347268008863,-41.3835260275347));
#22489=CARTESIAN_POINT('Ctrl Pts',(-23.7521538944338,20.3338232427365,-41.3826714960594));
#22490=CARTESIAN_POINT('Ctrl Pts',(-23.7441708246661,20.3333320741879,-41.3821805099766));
#22491=CARTESIAN_POINT('Ctrl Pts',(-23.4655252720813,20.31722907153,-41.365101337049));
#22492=CARTESIAN_POINT('Ctrl Pts',(-23.1939201396167,20.3358004696038,-41.350319306804));
#22493=CARTESIAN_POINT('Ctrl Pts',(-22.7803686303355,20.4172063535288,-41.326696484936));
#22494=CARTESIAN_POINT('Ctrl Pts',(-22.6351461133296,20.4565049949696,-41.3181880925579));
#22495=CARTESIAN_POINT('Ctrl Pts',(-22.4793226777967,20.5106073610616,-41.3085104758978));
#22496=CARTESIAN_POINT('Ctrl Pts',(-22.4654735885125,20.5155222059206,-41.3076455876232));
#22497=CARTESIAN_POINT('Ctrl Pts',(-22.4466104674205,20.5223620791715,-41.3064607775932));
#22498=CARTESIAN_POINT('Ctrl Pts',(-22.4415667895831,20.5242052215435,-41.3061433138948));
#22499=CARTESIAN_POINT('Ctrl Pts',(-22.4327959905675,20.5274352603334,-41.3055900794697));
#22500=CARTESIAN_POINT('Ctrl Pts',(-22.4290667769955,20.5288164690567,-41.3053544818526));
#22501=CARTESIAN_POINT('Ctrl Pts',(-22.4133112736714,20.5346851046373,-41.3043575263415));
#22502=CARTESIAN_POINT('Ctrl Pts',(-22.4013094091478,20.539237416211,-41.3035941857172));
#22503=CARTESIAN_POINT('Ctrl Pts',(-22.3879232405241,20.54440648237,-41.3027383035881));
#22504=CARTESIAN_POINT('Ctrl Pts',(-22.3865116834171,20.5449526978357,-41.3026479956832));
#22505=CARTESIAN_POINT('Ctrl Pts',(-22.3433282057686,20.5616979419278,-41.2998835033141));
#22506=CARTESIAN_POINT('Ctrl Pts',(-22.3018999252261,20.5787646337453,-41.2971819737084));
#22507=CARTESIAN_POINT('Ctrl Pts',(-22.2540071130783,20.599672757732,-41.2939962608039));
#22508=CARTESIAN_POINT('Ctrl Pts',(-22.247182264298,20.6026804690377,-41.2935407897615));
#22509=CARTESIAN_POINT('Ctrl Pts',(-22.2363108311614,20.6075166468755,-41.2928128432412));
#22510=CARTESIAN_POINT('Ctrl Pts',(-22.2322574505955,20.6093298455147,-41.2925408925523));
#22511=CARTESIAN_POINT('Ctrl Pts',(-22.2251116970178,20.6125440954311,-41.2920605119716));
#22512=CARTESIAN_POINT('Ctrl Pts',(-22.2220177597086,20.6139416696488,-41.2918522020798));
#22513=CARTESIAN_POINT('Ctrl Pts',(-22.2156271802226,20.616840549802,-41.2914212766334));
#22514=CARTESIAN_POINT('Ctrl Pts',(-22.212330850669,20.6183425297379,-41.2911986380487));
#22515=CARTESIAN_POINT('Ctrl Pts',(-22.2039019268377,20.6222003626003,-41.2906284046718));
#22516=CARTESIAN_POINT('Ctrl Pts',(-22.1987729956677,20.62456414788,-41.2902805360312));
#22517=CARTESIAN_POINT('Ctrl Pts',(-22.1782399960408,20.634092764969,-41.2888843118443));
#22518=CARTESIAN_POINT('Ctrl Pts',(-22.1628866942515,20.6413657689669,-41.2878322121485));
#22519=CARTESIAN_POINT('Ctrl Pts',(-21.9669040196301,20.736109133789,-41.274296651749));
#22520=CARTESIAN_POINT('Ctrl Pts',(-21.7948053974029,20.840128202668,-41.2612126617682));
#22521=CARTESIAN_POINT('Ctrl Pts',(-21.4588321651595,21.0886886834058,-41.2332023353009));
#22522=CARTESIAN_POINT('Ctrl Pts',(-21.2976670178716,21.2352592402422,-41.2182828203036));
#22523=CARTESIAN_POINT('Ctrl Pts',(-21.1442591332912,21.4060826185995,-41.2031511624606));
#22524=CARTESIAN_POINT('Ctrl Pts',(-21.1360931729729,21.4152809985134,-41.2023427174215));
#22525=CARTESIAN_POINT('Ctrl Pts',(-21.116767070109,21.4373031580937,-41.2004226858236));
#22526=CARTESIAN_POINT('Ctrl Pts',(-21.1056552224726,21.4501690655643,-41.1993133157525));
#22527=CARTESIAN_POINT('Ctrl Pts',(-21.0601424422341,21.5037170015254,-41.1947489149165));
#22528=CARTESIAN_POINT('Ctrl Pts',(-21.0266487222162,21.5451638607388,-41.1913405167319));
#22529=CARTESIAN_POINT('Ctrl Pts',(-20.9906872093283,21.5919940939217,-41.1876423650181));
#22530=CARTESIAN_POINT('Ctrl Pts',(-20.9871908378303,21.5965725417172,-41.1872823913285));
#22531=CARTESIAN_POINT('Ctrl Pts',(-20.9823136927706,21.602994719438,-41.1867796981482));
#22532=CARTESIAN_POINT('Ctrl Pts',(-20.9809226175676,21.6048305568257,-41.1866362541777));
#22533=CARTESIAN_POINT('Ctrl Pts',(-20.9783822909749,21.6081905678924,-41.1863741873715));
#22534=CARTESIAN_POINT('Ctrl Pts',(-20.9772324240969,21.6097142732977,-41.1862555207826));
#22535=CARTESIAN_POINT('Ctrl Pts',(-20.974901042143,21.6128093369461,-41.1860148350656));
#22536=CARTESIAN_POINT('Ctrl Pts',(-20.9737196107308,21.6143807552455,-41.1858928219053));
#22537=CARTESIAN_POINT('Ctrl Pts',(-20.9708251933189,21.6182379542092,-41.1855937849705));
#22538=CARTESIAN_POINT('Ctrl Pts',(-20.9691138027421,21.6205249385798,-41.1854168743607));
#22539=CARTESIAN_POINT('Ctrl Pts',(-20.9628961227953,21.628856886901,-41.1847737674746));
#22540=CARTESIAN_POINT('Ctrl Pts',(-20.9584079644878,21.6349154457887,-41.184308838526));
#22541=CARTESIAN_POINT('Ctrl Pts',(-20.8571208722336,21.7726507252989,-41.1737989198239));
#22542=CARTESIAN_POINT('Ctrl Pts',(-20.77044005158,21.9115074401729,-41.1644338798672));
#22543=CARTESIAN_POINT('Ctrl Pts',(-20.6130449901211,22.2123702043084,-41.145309559751));
#22544=CARTESIAN_POINT('Ctrl Pts',(-20.544352601722,22.3748023577325,-41.1355988020526));
#22545=CARTESIAN_POINT('Ctrl Pts',(-20.4684540834213,22.6052322037622,-41.1218151630692));
#22546=CARTESIAN_POINT('Ctrl Pts',(-20.4496006420701,22.6690588618789,-41.1179987580406));
#22547=CARTESIAN_POINT('Ctrl Pts',(-20.407213325427,22.8308340946823,-41.1082718354867));
#22548=CARTESIAN_POINT('Ctrl Pts',(-20.3862718482243,22.929381060805,-41.1022963742722));
#22549=CARTESIAN_POINT('Ctrl Pts',(-20.3684585423071,23.0380096054786,-41.0955963437874));
#22550=CARTESIAN_POINT('Ctrl Pts',(-20.3669789634239,23.0472861382102,-41.0950233108014));
#22551=CARTESIAN_POINT('Ctrl Pts',(-20.3648450352697,23.0610519343051,-41.094171629853));
#22552=CARTESIAN_POINT('Ctrl Pts',(-20.3641595643392,23.0655363819819,-41.0938939700616));
#22553=CARTESIAN_POINT('Ctrl Pts',(-20.3630035087695,23.073207872309,-41.093418616612));
#22554=CARTESIAN_POINT('Ctrl Pts',(-20.3625282286861,23.0763942099552,-41.093221072174));
#22555=CARTESIAN_POINT('Ctrl Pts',(-20.361613823296,23.0825881346818,-41.0928368546349));
#22556=CARTESIAN_POINT('Ctrl Pts',(-20.3611741734397,23.0855956413501,-41.0926501984311));
#22557=CARTESIAN_POINT('Ctrl Pts',(-20.360134257406,23.0927803815169,-41.0922040562289));
#22558=CARTESIAN_POINT('Ctrl Pts',(-20.3595379414966,23.0969581728459,-41.091944445281));
#22559=CARTESIAN_POINT('Ctrl Pts',(-20.3578118742822,23.1092231779174,-41.091181731827));
#22560=CARTESIAN_POINT('Ctrl Pts',(-20.3567046581239,23.1173134837474,-41.0906779160879));
#22561=CARTESIAN_POINT('Ctrl Pts',(-20.3479972685934,23.1827887965849,-41.0865946353172));
#22562=CARTESIAN_POINT('Ctrl Pts',(-20.3419141287191,23.2403616559554,-41.0829674321972));
#22563=CARTESIAN_POINT('Ctrl Pts',(-20.3260890129233,23.4419729159951,-41.0701255465557));
#22564=CARTESIAN_POINT('Ctrl Pts',(-20.3244759724534,23.5864592719757,-41.060664015175));
#22565=CARTESIAN_POINT('Ctrl Pts',(-20.3421994921574,23.9027616759515,-41.0394827368443));
#22566=CARTESIAN_POINT('Ctrl Pts',(-20.3656586222808,24.0739178112076,-41.0277107909783));
#22567=CARTESIAN_POINT('Ctrl Pts',(-20.419335767569,24.3180283047237,-41.0109317457834));
#22568=CARTESIAN_POINT('Ctrl Pts',(-20.4386974460152,24.3930727115073,-41.0057784802));
#22569=CARTESIAN_POINT('Ctrl Pts',(-20.4625734306141,24.4735057780515,-41.0003077128355));
#22570=CARTESIAN_POINT('Ctrl Pts',(-20.4644189794074,24.4796556073032,-40.9998897642706));
#22571=CARTESIAN_POINT('Ctrl Pts',(-20.4819635472328,24.5374901057151,-40.9959627361969));
#22572=CARTESIAN_POINT('Ctrl Pts',(-20.4989424691347,24.5887818219202,-40.9925059319402));
#22573=CARTESIAN_POINT('Ctrl Pts',(-20.5189639438809,24.6445258820784,-40.9887960581018));
#22574=CARTESIAN_POINT('Ctrl Pts',(-20.5207356915099,24.6494214831798,-40.988470648904));
#22575=CARTESIAN_POINT('Ctrl Pts',(-20.5233821793103,24.6566791114033,-40.9879888569771));
#22576=CARTESIAN_POINT('Ctrl Pts',(-20.5242478264575,24.6590444104607,-40.9878319364289));
#22577=CARTESIAN_POINT('Ctrl Pts',(-20.5257337623024,24.6630898889978,-40.9875637187772));
#22578=CARTESIAN_POINT('Ctrl Pts',(-20.5263526785113,24.6647705657205,-40.9874523393662));
#22579=CARTESIAN_POINT('Ctrl Pts',(-20.5275620598334,24.6680462364788,-40.9872353584309));
#22580=CARTESIAN_POINT('Ctrl Pts',(-20.5281523849009,24.6696412746679,-40.9871297491306));
#22581=CARTESIAN_POINT('Ctrl Pts',(-20.5295817197724,24.6734939167906,-40.9868747718376));
#22582=CARTESIAN_POINT('Ctrl Pts',(-20.5304220000345,24.6757510538329,-40.98672548065));
#22583=CARTESIAN_POINT('Ctrl Pts',(-20.5329691598665,24.6825697743285,-40.986274749046));
#22584=CARTESIAN_POINT('Ctrl Pts',(-20.5346838605444,24.6871284590463,-40.9859737774661));
#22585=CARTESIAN_POINT('Ctrl Pts',(-20.5517009973861,24.7320606546993,-40.9830107417448));
#22586=CARTESIAN_POINT('Ctrl Pts',(-20.5678038982715,24.7721290975503,-40.9803960175176));
#22587=CARTESIAN_POINT('Ctrl Pts',(-20.6175619192247,24.8890903030063,-40.972811274157));
#22588=CARTESIAN_POINT('Ctrl Pts',(-20.6534223947086,24.9650098056607,-40.9679494360663));
#22589=CARTESIAN_POINT('Ctrl Pts',(-20.7613381090476,25.1721201853498,-40.9546304121617));
#22590=CARTESIAN_POINT('Ctrl Pts',(-20.8396240128365,25.2998224030676,-40.9463463719579));
#22591=CARTESIAN_POINT('Ctrl Pts',(-20.9924913106465,25.5141491800164,-40.9315988283507));
#22592=CARTESIAN_POINT('Ctrl Pts',(-21.0633262226755,25.6031109674793,-40.925188582805));
#22593=CARTESIAN_POINT('Ctrl Pts',(-21.2180228873768,25.7776091955496,-40.9117283524356));
#22594=CARTESIAN_POINT('Ctrl Pts',(-21.302246410084,25.8625838599812,-40.9046723818301));
#22595=CARTESIAN_POINT('Ctrl Pts',(-21.3989027274113,25.9498202505893,-40.8967499969482));
#22596=CARTESIAN_POINT('Ctrl Pts',(-21.4068522424466,25.9569237626098,-40.8960996742361));
#22597=CARTESIAN_POINT('Ctrl Pts',(-21.4180584652827,25.9668378350808,-40.8951846240528));
#22598=CARTESIAN_POINT('Ctrl Pts',(-21.4212858382461,25.9696815724559,-40.8949212867044));
#22599=CARTESIAN_POINT('Ctrl Pts',(-21.4268935991946,25.9746028340699,-40.8944640556367));
#22600=CARTESIAN_POINT('Ctrl Pts',(-21.4292713728239,25.9766833401997,-40.8942702865844));
#22601=CARTESIAN_POINT('Ctrl Pts',(-21.4342226063569,25.9810027354216,-40.8938670148815));
#22602=CARTESIAN_POINT('Ctrl Pts',(-21.4367965676254,25.9832410408421,-40.893657488353));
#22603=CARTESIAN_POINT('Ctrl Pts',(-21.4428613753187,25.9884980844153,-40.8931640762106));
#22604=CARTESIAN_POINT('Ctrl Pts',(-21.4463551552772,25.9915134129778,-40.8928800497575));
#22605=CARTESIAN_POINT('Ctrl Pts',(-21.4575313264692,26.0011172663696,-40.8919721618911));
#22606=CARTESIAN_POINT('Ctrl Pts',(-21.4652382245715,26.0076770627464,-40.8913471164866));
#22607=CARTESIAN_POINT('Ctrl Pts',(-21.4833625541543,26.022957113248,-40.8898795049966));
#22608=CARTESIAN_POINT('Ctrl Pts',(-21.493804420512,26.0316479624535,-40.8890357473646));
#22609=CARTESIAN_POINT('Ctrl Pts',(-21.5297999024927,26.0612240389298,-40.8861329518472));
#22610=CARTESIAN_POINT('Ctrl Pts',(-21.5556185344741,26.0817820740018,-40.8840608032956));
#22611=CARTESIAN_POINT('Ctrl Pts',(-21.671582268812,26.1712425756115,-40.8747947891684));
#22612=CARTESIAN_POINT('Ctrl Pts',(-21.7650044344306,26.235745991501,-40.8674337730804));
#22613=CARTESIAN_POINT('Ctrl Pts',(-21.9312387053325,26.3380100516388,-40.8545249368777));
#22614=CARTESIAN_POINT('Ctrl Pts',(-22.002428899923,26.3781543765597,-40.8490530641783));
#22615=CARTESIAN_POINT('Ctrl Pts',(-22.0750362323924,26.4155368863044,-40.843547806833));
#22616=CARTESIAN_POINT('Origin',(-23.5502525316942,23.5502525316942,-77.3107734492734));
#22617=CARTESIAN_POINT('',(-22.0750358008163,26.4155366641038,-39.3444748119239));
#22618=CARTESIAN_POINT('',(-22.0750360153868,26.4155367745772,-39.5898217886697));
#22619=CARTESIAN_POINT('',(-22.0750360153461,26.4155367745563,-77.3107734492734));
#22620=CARTESIAN_POINT('Ctrl Pts',(-22.0750358008163,26.4155366641038,-39.3444748119239));
#22621=CARTESIAN_POINT('Ctrl Pts',(-22.0193043812446,26.3868428526741,-39.3486299213752));
#22622=CARTESIAN_POINT('Ctrl Pts',(-21.964396741262,26.3565161533716,-39.3528254761847));
#22623=CARTESIAN_POINT('Ctrl Pts',(-21.8092759268395,26.2648266674662,-39.3649499025387));
#22624=CARTESIAN_POINT('Ctrl Pts',(-21.7115103339792,26.1995805190266,-39.3729312042456));
#22625=CARTESIAN_POINT('Ctrl Pts',(-21.488195273045,26.032219219904,-39.3917525180478));
#22626=CARTESIAN_POINT('Ctrl Pts',(-21.3663191215635,25.9256868952839,-39.4025170211158));
#22627=CARTESIAN_POINT('Ctrl Pts',(-21.2486247535757,25.806059475927,-39.4130327228697));
#22628=CARTESIAN_POINT('Ctrl Pts',(-21.2443233526389,25.8016623169899,-39.4134172089316));
#22629=CARTESIAN_POINT('Ctrl Pts',(-21.2382020459838,25.7953687918453,-39.4139645715471));
#22630=CARTESIAN_POINT('Ctrl Pts',(-21.2363718641137,25.7934825079525,-39.4141282509411));
#22631=CARTESIAN_POINT('Ctrl Pts',(-21.2332165365611,25.7902224874891,-39.4144104839769));
#22632=CARTESIAN_POINT('Ctrl Pts',(-21.2318903019685,25.7888498106751,-39.4145291236578));
#22633=CARTESIAN_POINT('Ctrl Pts',(-21.229342977327,25.7862085918987,-39.4147570201795));
#22634=CARTESIAN_POINT('Ctrl Pts',(-21.2281217096894,25.7849402298415,-39.4148662912695));
#22635=CARTESIAN_POINT('Ctrl Pts',(-21.2252350719002,25.7819373562412,-39.4151245951554));
#22636=CARTESIAN_POINT('Ctrl Pts',(-21.2235705994816,25.7802019775032,-39.4152735572443));
#22637=CARTESIAN_POINT('Ctrl Pts',(-21.2186240262652,25.7750331132523,-39.415716318974));
#22638=CARTESIAN_POINT('Ctrl Pts',(-21.2153475536939,25.7715942136061,-39.4160096810171));
#22639=CARTESIAN_POINT('Ctrl Pts',(-21.1854690283587,25.7400953507706,-39.4186858391908));
#22640=CARTESIAN_POINT('Ctrl Pts',(-21.1593649343925,25.711564497402,-39.4210308816463));
#22641=CARTESIAN_POINT('Ctrl Pts',(-21.1316739996977,25.6801834158288,-39.4235351543124));
#22642=CARTESIAN_POINT('Ctrl Pts',(-21.1295722750046,25.6777944893671,-39.4237253334619));
#22643=CARTESIAN_POINT('Ctrl Pts',(-21.1261770698113,25.6739237836257,-39.4240327359742));
#22644=CARTESIAN_POINT('Ctrl Pts',(-21.1248814070281,25.6724439318412,-39.4241500880913));
#22645=CARTESIAN_POINT('Ctrl Pts',(-21.1179755339058,25.6645417477779,-39.424775807182));
#22646=CARTESIAN_POINT('Ctrl Pts',(-21.1123894228983,25.6580982919244,-39.4252827691741));
#22647=CARTESIAN_POINT('Ctrl Pts',(-20.9810475646201,25.5053778040405,-39.4372241754453));
#22648=CARTESIAN_POINT('Ctrl Pts',(-20.868637098761,25.34810803634,-39.4479312832544));
#22649=CARTESIAN_POINT('Ctrl Pts',(-20.6946046782655,25.051633148377,-39.4671429162764));
#22650=CARTESIAN_POINT('Ctrl Pts',(-20.6274775815421,24.9163604260466,-39.4755924773899));
#22651=CARTESIAN_POINT('Ctrl Pts',(-20.5401133729809,24.7041049465896,-39.4888726865368));
#22652=CARTESIAN_POINT('Ctrl Pts',(-20.5128326893871,24.6302490213189,-39.4934952468059));
#22653=CARTESIAN_POINT('Ctrl Pts',(-20.4801244786856,24.5306175908253,-39.4997723622537));
#22654=CARTESIAN_POINT('Ctrl Pts',(-20.472267921572,24.5056647934783,-39.5013477594362));
#22655=CARTESIAN_POINT('Ctrl Pts',(-20.4614172952391,24.4696789970701,-39.5036255687295));
#22656=CARTESIAN_POINT('Ctrl Pts',(-20.4581766566244,24.4587209795667,-39.5043199545695));
#22657=CARTESIAN_POINT('Ctrl Pts',(-20.452536819609,24.4392704200904,-39.5055539605528));
#22658=CARTESIAN_POINT('Ctrl Pts',(-20.4501140842354,24.4307847814935,-39.5060928092514));
#22659=CARTESIAN_POINT('Ctrl Pts',(-20.4465661128762,24.4181618348877,-39.5068951490833));
#22660=CARTESIAN_POINT('Ctrl Pts',(-20.4454142173505,24.4140320095859,-39.5071577707357));
#22661=CARTESIAN_POINT('Ctrl Pts',(-20.4434107258247,24.4067932176488,-39.5076183137289));
#22662=CARTESIAN_POINT('Ctrl Pts',(-20.4425555449002,24.4036852423064,-39.5078161180339));
#22663=CARTESIAN_POINT('Ctrl Pts',(-20.4408609343673,24.3974902147152,-39.508210536894));
#22664=CARTESIAN_POINT('Ctrl Pts',(-20.4400214355155,24.3944031848937,-39.5084071489515));
#22665=CARTESIAN_POINT('Ctrl Pts',(-20.4380242926073,24.3870158097381,-39.5088778188505));
#22666=CARTESIAN_POINT('Ctrl Pts',(-20.4368709652479,24.3827143128325,-39.5091520167178));
#22667=CARTESIAN_POINT('Ctrl Pts',(-20.4327555908068,24.3672372640745,-39.5101391018188));
#22668=CARTESIAN_POINT('Ctrl Pts',(-20.4298447974355,24.356048284828,-39.5108536504688));
#22669=CARTESIAN_POINT('Ctrl Pts',(-20.382191737911,24.1687409501885,-39.522831920012));
#22670=CARTESIAN_POINT('Ctrl Pts',(-20.3523712358977,23.9891964742879,-39.5345858927473));
#22671=CARTESIAN_POINT('Ctrl Pts',(-20.3273887690622,23.6779774345387,-39.5553802070713));
#22672=CARTESIAN_POINT('Ctrl Pts',(-20.3248606230775,23.5473228731805,-39.5642274684996));
#22673=CARTESIAN_POINT('Ctrl Pts',(-20.3378158785744,23.2345415298741,-39.5854097861483));
#22674=CARTESIAN_POINT('Ctrl Pts',(-20.3608440264336,23.0531484861227,-39.5977025204903));
#22675=CARTESIAN_POINT('Ctrl Pts',(-20.4024449319433,22.8591100853893,-39.6102548582153));
#22676=CARTESIAN_POINT('Ctrl Pts',(-20.4058945269916,22.8435819370975,-39.6112549994919));
#22677=CARTESIAN_POINT('Ctrl Pts',(-20.4103001093683,22.8244216727545,-39.6124831234204));
#22678=CARTESIAN_POINT('Ctrl Pts',(-20.4111475807279,22.820765206636,-39.6127172247817));
#22679=CARTESIAN_POINT('Ctrl Pts',(-20.412490969693,22.8150147653623,-39.6130849585368));
#22680=CARTESIAN_POINT('Ctrl Pts',(-20.4129825965446,22.8129198068781,-39.6132188382784));
#22681=CARTESIAN_POINT('Ctrl Pts',(-20.4139045632166,22.8090086671001,-39.6134686115778));
#22682=CARTESIAN_POINT('Ctrl Pts',(-20.4143343796771,22.807192379318,-39.6135845343494));
#22683=CARTESIAN_POINT('Ctrl Pts',(-20.4153017471695,22.8031203356083,-39.6138442744832));
#22684=CARTESIAN_POINT('Ctrl Pts',(-20.4158401539492,22.8008647908342,-39.6139880412715));
#22685=CARTESIAN_POINT('Ctrl Pts',(-20.4172127016631,22.7951421407762,-39.6143525348038));
#22686=CARTESIAN_POINT('Ctrl Pts',(-20.4180501660424,22.7916758250126,-39.6145730692289));
#22687=CARTESIAN_POINT('Ctrl Pts',(-20.4226672552121,22.7727034177944,-39.6157788220425));
#22688=CARTESIAN_POINT('Ctrl Pts',(-20.4265563601074,22.7572238193735,-39.6167577938703));
#22689=CARTESIAN_POINT('Ctrl Pts',(-20.5035058299617,22.4602976033242,-39.6354549986704));
#22690=CARTESIAN_POINT('Ctrl Pts',(-20.6142228998984,22.1899360936725,-39.6511598327141));
#22691=CARTESIAN_POINT('Ctrl Pts',(-20.861312833267,21.7622510921412,-39.6789569481323));
#22692=CARTESIAN_POINT('Ctrl Pts',(-20.9792582517433,21.5964574043754,-39.6906304146278));
#22693=CARTESIAN_POINT('Ctrl Pts',(-21.117490810232,21.4365216070641,-39.7034800319533));
#22694=CARTESIAN_POINT('Ctrl Pts',(-21.1230042007556,21.4301927322972,-39.7039912523034));
#22695=CARTESIAN_POINT('Ctrl Pts',(-21.1318310673715,21.4201398515844,-39.7048077050071));
#22696=CARTESIAN_POINT('Ctrl Pts',(-21.1351285936242,21.4164018404831,-39.7051122724734));
#22697=CARTESIAN_POINT('Ctrl Pts',(-21.1414142525737,21.4093097752986,-39.7056920019537));
#22698=CARTESIAN_POINT('Ctrl Pts',(-21.1444007542759,21.4059542861396,-39.7059670952487));
#22699=CARTESIAN_POINT('Ctrl Pts',(-21.1496229120234,21.4001115651206,-39.7064475102501));
#22700=CARTESIAN_POINT('Ctrl Pts',(-21.1518554475422,21.3976215429798,-39.7066527002497));
#22701=CARTESIAN_POINT('Ctrl Pts',(-21.1562025901155,21.3927881860953,-39.7070518689786));
#22702=CARTESIAN_POINT('Ctrl Pts',(-21.1583167727293,21.3904444730533,-39.7072458296332));
#22703=CARTESIAN_POINT('Ctrl Pts',(-21.1633124635531,21.3849227469965,-39.7077037482568));
#22704=CARTESIAN_POINT('Ctrl Pts',(-21.1661968759341,21.3817473794389,-39.7079678293286));
#22705=CARTESIAN_POINT('Ctrl Pts',(-21.1762269111128,21.370749798858,-39.7088850526205));
#22706=CARTESIAN_POINT('Ctrl Pts',(-21.1834047016666,21.36295713445,-39.7095395646226));
#22707=CARTESIAN_POINT('Ctrl Pts',(-21.2699943751491,21.2698751910248,-39.7174132592279));
#22708=CARTESIAN_POINT('Ctrl Pts',(-21.3539280994796,21.1889284455533,-39.7248292125155));
#22709=CARTESIAN_POINT('Ctrl Pts',(-21.6497989526624,20.9330332595097,-39.7503226063137));
#22710=CARTESIAN_POINT('Ctrl Pts',(-21.8796548596196,20.7806628045816,-39.769218612152));
#22711=CARTESIAN_POINT('Ctrl Pts',(-22.1653336071807,20.6399190007228,-39.7904829088811));
#22712=CARTESIAN_POINT('Ctrl Pts',(-22.205075492554,20.6213379366103,-39.793392149016));
#22713=CARTESIAN_POINT('Ctrl Pts',(-22.2923759542161,20.5826730770439,-39.7996600518868));
#22714=CARTESIAN_POINT('Ctrl Pts',(-22.340064500163,20.5629080759267,-39.8030065816337));
#22715=CARTESIAN_POINT('Ctrl Pts',(-22.4112024407974,20.5354075762282,-39.8078646106639));
#22716=CARTESIAN_POINT('Ctrl Pts',(-22.4342968984392,20.5267829469499,-39.8094212254556));
#22717=CARTESIAN_POINT('Ctrl Pts',(-22.4615170774918,20.51697196314,-39.811230049917));
#22718=CARTESIAN_POINT('Ctrl Pts',(-22.4655481879374,20.5155280987436,-39.8114972613409));
#22719=CARTESIAN_POINT('Ctrl Pts',(-22.4717177917273,20.5133321317214,-39.8119052023128));
#22720=CARTESIAN_POINT('Ctrl Pts',(-22.4738542010116,20.5125742513514,-39.8120462762675));
#22721=CARTESIAN_POINT('Ctrl Pts',(-22.4777319669671,20.5112032380905,-39.8123019946953));
#22722=CARTESIAN_POINT('Ctrl Pts',(-22.4794730441465,20.5105893497264,-39.8124166841769));
#22723=CARTESIAN_POINT('Ctrl Pts',(-22.4830059943339,20.5093470749909,-39.8126491547138));
#22724=CARTESIAN_POINT('Ctrl Pts',(-22.4847978881922,20.5087187786674,-39.8127669301088));
#22725=CARTESIAN_POINT('Ctrl Pts',(-22.4899537820387,20.5069160699025,-39.8131054323337));
#22726=CARTESIAN_POINT('Ctrl Pts',(-22.4933191893341,20.5057456474368,-39.8133259203452));
#22727=CARTESIAN_POINT('Ctrl Pts',(-22.5080720104234,20.5006423166081,-39.8142904691134));
#22728=CARTESIAN_POINT('Ctrl Pts',(-22.5194796776835,20.4967676312706,-39.8150311016987));
#22729=CARTESIAN_POINT('Ctrl Pts',(-22.5341846714721,20.4918647883519,-39.8159794463193));
#22730=CARTESIAN_POINT('Ctrl Pts',(-22.5374620964976,20.4907779003529,-39.8161904063017));
#22731=CARTESIAN_POINT('Ctrl Pts',(-22.5417188482794,20.4893738291756,-39.8164638847554));
#22732=CARTESIAN_POINT('Ctrl Pts',(-22.5426965737359,20.4890518499832,-39.8165266640416));
#22733=CARTESIAN_POINT('Ctrl Pts',(-22.8524420315311,20.3872126447571,-39.8364040873027));
#22734=CARTESIAN_POINT('Ctrl Pts',(-23.1748481546112,20.33296841668,-39.8537182973952));
#22735=CARTESIAN_POINT('Ctrl Pts',(-23.6553486680242,20.3254701005996,-39.8809858788801));
#22736=CARTESIAN_POINT('Ctrl Pts',(-23.8106822747038,20.3342870950583,-39.8899977857389));
#22737=CARTESIAN_POINT('Ctrl Pts',(-23.9798908472098,20.3562329285497,-39.9003023449612));
#22738=CARTESIAN_POINT('Ctrl Pts',(-23.995005781739,20.3583025255617,-39.9012270003272));
#22739=CARTESIAN_POINT('Ctrl Pts',(-24.0176898902132,20.3615727734449,-39.9026211948382));
#22740=CARTESIAN_POINT('Ctrl Pts',(-24.0252705502291,20.3626932514166,-39.9030882037144));
#22741=CARTESIAN_POINT('Ctrl Pts',(-24.0374753019795,20.3645417089266,-39.9038418671412));
#22742=CARTESIAN_POINT('Ctrl Pts',(-24.0421019609835,20.3652527494764,-39.9041279848361));
#22743=CARTESIAN_POINT('Ctrl Pts',(-24.0509455767538,20.3666315954283,-39.9046756822619));
#22744=CARTESIAN_POINT('Ctrl Pts',(-24.0551627907752,20.3672977061904,-39.9049372077152));
#22745=CARTESIAN_POINT('Ctrl Pts',(-24.0626441051334,20.3684946254285,-39.9054017738816));
#22746=CARTESIAN_POINT('Ctrl Pts',(-24.0659087418275,20.3690220824129,-39.9056047077545));
#22747=CARTESIAN_POINT('Ctrl Pts',(-24.0723514701997,20.3700731915604,-39.9060056130027));
#22748=CARTESIAN_POINT('Ctrl Pts',(-24.075529600815,20.3705965852856,-39.9062035759461));
#22749=CARTESIAN_POINT('Ctrl Pts',(-24.0831801202355,20.3718683022208,-39.9066806055717));
#22750=CARTESIAN_POINT('Ctrl Pts',(-24.0876517159908,20.3726213005435,-39.9069598208863));
#22751=CARTESIAN_POINT('Ctrl Pts',(-24.1013743183089,20.3749619244198,-39.9078179236273));
#22752=CARTESIAN_POINT('Ctrl Pts',(-24.1106199281166,20.3765805192833,-39.9083977969088));
#22753=CARTESIAN_POINT('Ctrl Pts',(-24.2186704867407,20.3959834081086,-39.9151950639356));
#22754=CARTESIAN_POINT('Ctrl Pts',(-24.3165895560363,20.4183329591346,-39.9215580347125));
#22755=CARTESIAN_POINT('Ctrl Pts',(-24.4739914952224,20.462082820137,-39.9321359420316));
#22756=CARTESIAN_POINT('Ctrl Pts',(-24.5341740796881,20.4807275748041,-39.936265418512));
#22757=CARTESIAN_POINT('Ctrl Pts',(-24.7984724093166,20.5711794953779,-39.9547626052912));
#22758=CARTESIAN_POINT('Ctrl Pts',(-24.9955952148721,20.6616712136987,-39.9695795652277));
#22759=CARTESIAN_POINT('Ctrl Pts',(-25.2913012167031,20.8353140012914,-39.9925530879096));
#22760=CARTESIAN_POINT('Ctrl Pts',(-25.3966028411608,20.9057978413637,-40.0008910013439));
#22761=CARTESIAN_POINT('Ctrl Pts',(-25.5038363777757,20.9871116772185,-40.0093405600064));
#22762=CARTESIAN_POINT('Ctrl Pts',(-25.5101592793117,20.9919432408942,-40.0098386045528));
#22763=CARTESIAN_POINT('Ctrl Pts',(-25.5187743392916,20.9985770123843,-40.0105168851808));
#22764=CARTESIAN_POINT('Ctrl Pts',(-25.5210819748955,21.0003589321878,-40.0106985389872));
#22765=CARTESIAN_POINT('Ctrl Pts',(-25.5249416578276,21.0033476879949,-40.0110023114422));
#22766=CARTESIAN_POINT('Ctrl Pts',(-25.5264950187851,21.0045528125608,-40.0111245518396));
#22767=CARTESIAN_POINT('Ctrl Pts',(-25.5295542536041,21.0069307079442,-40.011365263836));
#22768=CARTESIAN_POINT('Ctrl Pts',(-25.5310601885078,21.0081033951837,-40.0114837410902));
#22769=CARTESIAN_POINT('Ctrl Pts',(-25.5343807105304,21.0106938623091,-40.0117449467312));
#22770=CARTESIAN_POINT('Ctrl Pts',(-25.5361948247782,21.012112253081,-40.0118876313892));
#22771=CARTESIAN_POINT('Ctrl Pts',(-25.5425395827863,21.017083958303,-40.0123865956124));
#22772=CARTESIAN_POINT('Ctrl Pts',(-25.5470622576685,21.0206474963903,-40.0127421479018));
#22773=CARTESIAN_POINT('Ctrl Pts',(-25.5932603644229,21.0572493383338,-40.0163730878217));
#22774=CARTESIAN_POINT('Ctrl Pts',(-25.6341244494885,21.0913046739964,-40.0195769088653));
#22775=CARTESIAN_POINT('Ctrl Pts',(-25.6773037562032,21.1291394693697,-40.0229768807352));
#22776=CARTESIAN_POINT('Ctrl Pts',(-25.6804723707524,21.1319269105535,-40.0232264669171));
#22777=CARTESIAN_POINT('Ctrl Pts',(-25.6893365278733,21.1397556796846,-40.0239249552417));
#22778=CARTESIAN_POINT('Ctrl Pts',(-25.6950197433927,21.144810986827,-40.0243731064914));
#22779=CARTESIAN_POINT('Ctrl Pts',(-25.7254692191221,21.1720899682558,-40.0267762598433));
#22780=CARTESIAN_POINT('Ctrl Pts',(-25.7499087912535,21.1946767439125,-40.028712438279));
#22781=CARTESIAN_POINT('Ctrl Pts',(-25.8851971439204,21.3236507005305,-40.0395012291548));
#22782=CARTESIAN_POINT('Ctrl Pts',(-25.9886829489201,21.4374854211448,-40.0480344162214));
#22783=CARTESIAN_POINT('Ctrl Pts',(-26.175137740566,21.6746193257529,-40.0648975549305));
#22784=CARTESIAN_POINT('Ctrl Pts',(-26.2584899917043,21.7971216767046,-40.0732048404906));
#22785=CARTESIAN_POINT('Ctrl Pts',(-26.3682548041575,21.9850584135228,-40.0858199247245));
#22786=CARTESIAN_POINT('Ctrl Pts',(-26.4014231165206,22.0463260930644,-40.0899119294625));
#22787=CARTESIAN_POINT('Ctrl Pts',(-26.4522654039221,22.1479773705553,-40.0967014799763));
#22788=CARTESIAN_POINT('Ctrl Pts',(-26.4711428138771,22.187735006646,-40.0993569430766));
#22789=CARTESIAN_POINT('Ctrl Pts',(-26.4923460979797,22.2348583649895,-40.1025086019364));
#22790=CARTESIAN_POINT('Ctrl Pts',(-26.4954676648637,22.2418626110948,-40.1029771586341));
#22791=CARTESIAN_POINT('Ctrl Pts',(-26.5002068949672,22.2525995094628,-40.1036956003655));
#22792=CARTESIAN_POINT('Ctrl Pts',(-26.5018425534703,22.2563242281902,-40.1039448677161));
#22793=CARTESIAN_POINT('Ctrl Pts',(-26.504680312456,22.2628197477584,-40.1043796269023));
#22794=CARTESIAN_POINT('Ctrl Pts',(-26.5058855809764,22.2655891661459,-40.1045650099888));
#22795=CARTESIAN_POINT('Ctrl Pts',(-26.508395158224,22.2713777995516,-40.1049525408));
#22796=CARTESIAN_POINT('Ctrl Pts',(-26.5096987412893,22.2743973236896,-40.1051547130781));
#22797=CARTESIAN_POINT('Ctrl Pts',(-26.5132851939323,22.2827397900305,-40.1057133539995));
#22798=CARTESIAN_POINT('Ctrl Pts',(-26.51555833157,22.288066879624,-40.1060701543683));
#22799=CARTESIAN_POINT('Ctrl Pts',(-26.5243847909365,22.3089071040138,-40.1074663342694));
#22800=CARTESIAN_POINT('Ctrl Pts',(-26.5308307446904,22.324465166293,-40.1085093607361));
#22801=CARTESIAN_POINT('Ctrl Pts',(-26.5435867323968,22.3559488229183,-40.1106217534887));
#22802=CARTESIAN_POINT('Ctrl Pts',(-26.5498923149257,22.371875623209,-40.1116912299134));
#22803=CARTESIAN_POINT('Ctrl Pts',(-26.5573628858436,22.3911935518822,-40.1129895902443));
#22804=CARTESIAN_POINT('Ctrl Pts',(-26.5586496618932,22.3945375549122,-40.1132143832554));
#22805=CARTESIAN_POINT('Ctrl Pts',(-26.5615812069348,22.4021939642269,-40.1137291661877));
#22806=CARTESIAN_POINT('Ctrl Pts',(-26.5632222912403,22.4065077645519,-40.11401927812));
#22807=CARTESIAN_POINT('Ctrl Pts',(-26.5654514358838,22.4124054483284,-40.1144160087214));
#22808=CARTESIAN_POINT('Ctrl Pts',(-26.5660475317198,22.4139863063961,-40.114522361005));
#22809=CARTESIAN_POINT('Ctrl Pts',(-26.5682404733335,22.4198159132048,-40.1149145841221));
#22810=CARTESIAN_POINT('Ctrl Pts',(-26.5698295801112,22.4240675501587,-40.1152007101685));
#22811=CARTESIAN_POINT('Ctrl Pts',(-26.5738306163833,22.4348416262432,-40.1159259644523));
#22812=CARTESIAN_POINT('Ctrl Pts',(-26.5762304172222,22.4413685173391,-40.1163654892191));
#22813=CARTESIAN_POINT('Ctrl Pts',(-26.5807171654634,22.4536944393504,-40.1171958495523));
#22814=CARTESIAN_POINT('Ctrl Pts',(-26.5828086427921,22.459491797797,-40.1175865354797));
#22815=CARTESIAN_POINT('Ctrl Pts',(-26.5862561019136,22.4691343567345,-40.1182365791334));
#22816=CARTESIAN_POINT('Ctrl Pts',(-26.5876214455889,22.4729762127876,-40.118495634177));
#22817=CARTESIAN_POINT('Ctrl Pts',(-26.5909282573542,22.4823373078819,-40.1191269971723));
#22818=CARTESIAN_POINT('Ctrl Pts',(-26.5928619880055,22.4878592478708,-40.1194995514436));
#22819=CARTESIAN_POINT('Ctrl Pts',(-26.6031367635958,22.5174579285306,-40.1214971895168));
#22820=CARTESIAN_POINT('Ctrl Pts',(-26.6112068981729,22.5416271630281,-40.1231307862509));
#22821=CARTESIAN_POINT('Ctrl Pts',(-26.6955735338472,22.8046387483594,-40.1409338551455));
#22822=CARTESIAN_POINT('Ctrl Pts',(-26.7440238002873,23.0514817893682,-40.1579746615357));
#22823=CARTESIAN_POINT('Ctrl Pts',(-26.7698317099746,23.3846965035763,-40.1805383707152));
#22824=CARTESIAN_POINT('Ctrl Pts',(-26.7730419584783,23.4682248964479,-40.186148437505));
#22825=CARTESIAN_POINT('Ctrl Pts',(-26.7729616907037,23.6367855573696,-40.1972739748567));
#22826=CARTESIAN_POINT('Ctrl Pts',(-26.7695585239657,23.7217583255444,-40.2027819157312));
#22827=CARTESIAN_POINT('Ctrl Pts',(-26.7622951592415,23.8128164386024,-40.2085079375289));
#22828=CARTESIAN_POINT('Ctrl Pts',(-26.7617731417886,23.8191261431661,-40.2089037955238));
#22829=CARTESIAN_POINT('Ctrl Pts',(-26.7610221302478,23.8278893790836,-40.2094522714681));
#22830=CARTESIAN_POINT('Ctrl Pts',(-26.7608089156665,23.830344194295,-40.2096057711108));
#22831=CARTESIAN_POINT('Ctrl Pts',(-26.7604371519985,23.834568238835,-40.2098696516874));
#22832=CARTESIAN_POINT('Ctrl Pts',(-26.7602799556067,23.8363375811637,-40.2099801091898));
#22833=CARTESIAN_POINT('Ctrl Pts',(-26.759951771976,23.8399971634916,-40.2102084148184));
#22834=CARTESIAN_POINT('Ctrl Pts',(-26.7597805780771,23.8418873790929,-40.210326250478));
#22835=CARTESIAN_POINT('Ctrl Pts',(-26.7593739622225,23.8463332528007,-40.2106032032153));
#22836=CARTESIAN_POINT('Ctrl Pts',(-26.759137156407,23.8488887898389,-40.2107622416241));
#22837=CARTESIAN_POINT('Ctrl Pts',(-26.7583548826092,23.8572224863665,-40.2112803671126));
#22838=CARTESIAN_POINT('Ctrl Pts',(-26.7577968545562,23.8629994983255,-40.2116387465621));
#22839=CARTESIAN_POINT('Ctrl Pts',(-26.7437398286368,24.0045294407308,-40.2203999202259));
#22840=CARTESIAN_POINT('Ctrl Pts',(-26.7216480144846,24.1393110578934,-40.2283235834077));
#22841=CARTESIAN_POINT('Ctrl Pts',(-26.6107496905108,24.6217035391429,-40.2564428437242));
#22842=CARTESIAN_POINT('Ctrl Pts',(-26.4727030976038,24.9552220863105,-40.2757435691211));
#22843=CARTESIAN_POINT('Ctrl Pts',(-26.2711447527167,25.2774840644441,-40.2987143824648));
#22844=CARTESIAN_POINT('Ctrl Pts',(-26.2595183758889,25.2956641726692,-40.3000251262651));
#22845=CARTESIAN_POINT('Ctrl Pts',(-26.244211932783,25.3190773355242,-40.3017330570757));
#22846=CARTESIAN_POINT('Ctrl Pts',(-26.2406974564878,25.3244184053037,-40.3021240303567));
#22847=CARTESIAN_POINT('Ctrl Pts',(-26.2350749947224,25.3329079276356,-40.3027476521517));
#22848=CARTESIAN_POINT('Ctrl Pts',(-26.2329772977947,25.3360632013388,-40.3029799128244));
#22849=CARTESIAN_POINT('Ctrl Pts',(-26.2291993335496,25.3417241885289,-40.3033974882909));
#22850=CARTESIAN_POINT('Ctrl Pts',(-26.2275211002365,25.3442312596081,-40.3035827260705));
#22851=CARTESIAN_POINT('Ctrl Pts',(-26.2235908134966,25.350084819525,-40.3040159428671));
#22852=CARTESIAN_POINT('Ctrl Pts',(-26.2213359962547,25.3534294388183,-40.3042640263814));
#22853=CARTESIAN_POINT('Ctrl Pts',(-26.2148664522571,25.3629870910404,-40.3049745396833));
#22854=CARTESIAN_POINT('Ctrl Pts',(-26.2106363067511,25.3691896103726,-40.3054375546134));
#22855=CARTESIAN_POINT('Ctrl Pts',(-26.183298377065,25.408974919158,-40.3084199682001));
#22856=CARTESIAN_POINT('Ctrl Pts',(-26.1595777154717,25.4421302171039,-40.310962721746));
#22857=CARTESIAN_POINT('Ctrl Pts',(-26.0871757867881,25.5393765933113,-40.3185977732205));
#22858=CARTESIAN_POINT('Ctrl Pts',(-26.0367188712131,25.6020998598379,-40.3237584064895));
#22859=CARTESIAN_POINT('Ctrl Pts',(-25.8841030917694,25.7779124274078,-40.3389285097516));
#22860=CARTESIAN_POINT('Ctrl Pts',(-25.7762127085705,25.8857224845346,-40.3491423694584));
#22861=CARTESIAN_POINT('Ctrl Pts',(-25.5144132645354,26.1126500919241,-40.3725695110983));
#22862=CARTESIAN_POINT('Ctrl Pts',(-25.3565121075421,26.2263028725007,-40.3857975470013));
#22863=CARTESIAN_POINT('Ctrl Pts',(-25.1842916925768,26.3280336335191,-40.3987360348031));
#22864=CARTESIAN_POINT('Ctrl Pts',(-25.1792434403606,26.3309971171321,-40.3991140323917));
#22865=CARTESIAN_POINT('Ctrl Pts',(-25.1685615708219,26.3372286408767,-40.3999111458774));
#22866=CARTESIAN_POINT('Ctrl Pts',(-25.1629260535916,26.3404933980867,-40.400330098746));
#22867=CARTESIAN_POINT('Ctrl Pts',(-25.127107343058,26.3610990577738,-40.4029826837996));
#22868=CARTESIAN_POINT('Ctrl Pts',(-25.0966532459377,26.3779679286133,-40.4051920149658));
#22869=CARTESIAN_POINT('Ctrl Pts',(-25.0618643214626,26.3965077182443,-40.4076591053477));
#22870=CARTESIAN_POINT('Ctrl Pts',(-25.0577936699645,26.3986658631789,-40.4079469097147));
#22871=CARTESIAN_POINT('Ctrl Pts',(-25.0516238190644,26.4019200136322,-40.4083818006319));
#22872=CARTESIAN_POINT('Ctrl Pts',(-25.0495280385203,26.4030224356301,-40.4085292926888));
#22873=CARTESIAN_POINT('Ctrl Pts',(-25.0458800917313,26.4049361974634,-40.4087856135165));
#22874=CARTESIAN_POINT('Ctrl Pts',(-25.0443284793919,26.4057485818574,-40.4088945090383));
#22875=CARTESIAN_POINT('Ctrl Pts',(-25.0410776524406,26.4074472563621,-40.4091223907735));
#22876=CARTESIAN_POINT('Ctrl Pts',(-25.0393783103464,26.4083332951952,-40.4092413605066));
#22877=CARTESIAN_POINT('Ctrl Pts',(-25.035357009636,26.4104254457452,-40.4095225282901));
#22878=CARTESIAN_POINT('Ctrl Pts',(-25.0330343638712,26.4116302500242,-40.409684642745));
#22879=CARTESIAN_POINT('Ctrl Pts',(-25.0252696727443,26.415645962449,-40.4102256576603));
#22880=CARTESIAN_POINT('Ctrl Pts',(-25.0198210385415,26.4184442066952,-40.4106037579009));
#22881=CARTESIAN_POINT('Ctrl Pts',(-25.0068620581773,26.4250529027084,-40.4114994534875));
#22882=CARTESIAN_POINT('Ctrl Pts',(-24.999344645047,26.428849505306,-40.412016199166));
#22883=CARTESIAN_POINT('Ctrl Pts',(-24.7280357745039,26.5645394972366,-40.4305668905324));
#22884=CARTESIAN_POINT('Ctrl Pts',(-24.4473474058066,26.6596556994222,-40.4464829212868));
#22885=CARTESIAN_POINT('Ctrl Pts',(-23.9588604612326,26.753392499944,-40.4744755421013));
#22886=CARTESIAN_POINT('Ctrl Pts',(-23.7570114492831,26.772720247831,-40.4861086074569));
#22887=CARTESIAN_POINT('Ctrl Pts',(-23.5421097332939,26.773016839029,-40.4991674843511));
#22888=CARTESIAN_POINT('Ctrl Pts',(-23.529519290729,26.7729604321195,-40.4999348546891));
#22889=CARTESIAN_POINT('Ctrl Pts',(-23.5123117633937,26.7727824986097,-40.5009868594883));
#22890=CARTESIAN_POINT('Ctrl Pts',(-23.5076940135634,26.7727248219926,-40.5012694895278));
#22891=CARTESIAN_POINT('Ctrl Pts',(-23.4998330520786,26.772609737263,-40.5017511675346));
#22892=CARTESIAN_POINT('Ctrl Pts',(-23.4965897640427,26.7725573576625,-40.5019500574627));
#22893=CARTESIAN_POINT('Ctrl Pts',(-23.4903152951151,26.7724465484567,-40.5023351388454));
#22894=CARTESIAN_POINT('Ctrl Pts',(-23.4872841061145,26.7723887378889,-40.5025213106258));
#22895=CARTESIAN_POINT('Ctrl Pts',(-23.4800891579364,26.7722413597989,-40.5029635481683));
#22896=CARTESIAN_POINT('Ctrl Pts',(-23.4759254895573,26.7721479983406,-40.5032197327881));
#22897=CARTESIAN_POINT('Ctrl Pts',(-23.4636362900537,26.7718486044526,-40.5039766576652));
#22898=CARTESIAN_POINT('Ctrl Pts',(-23.455511389138,26.7716199033696,-40.5044781089932));
#22899=CARTESIAN_POINT('Ctrl Pts',(-23.3962879282221,26.7697286214481,-40.5081407771957));
#22900=CARTESIAN_POINT('Ctrl Pts',(-23.3452369727204,26.7668811280424,-40.5113390353455));
#22901=CARTESIAN_POINT('Ctrl Pts',(-23.1766186828373,26.7534457544234,-40.5220468777366));
#22902=CARTESIAN_POINT('Ctrl Pts',(-23.05957666139,26.7376152056598,-40.5297163611454));
#22903=CARTESIAN_POINT('Ctrl Pts',(-22.6816014622723,26.6651793368112,-40.5552167909542));
#22904=CARTESIAN_POINT('Ctrl Pts',(-22.4268035424485,26.5826066103071,-40.5736589341423));
#22905=CARTESIAN_POINT('Ctrl Pts',(-22.1765026572863,26.4655602462323,-40.5918247588175));
#22906=CARTESIAN_POINT('Ctrl Pts',(-22.1679159917987,26.4614985676578,-40.5924478687849));
#22907=CARTESIAN_POINT('Ctrl Pts',(-22.1310407320159,26.4438558405741,-40.5951231116031));
#22908=CARTESIAN_POINT('Ctrl Pts',(-22.1029339564756,26.4299002722503,-40.5971604721212));
#22909=CARTESIAN_POINT('Ctrl Pts',(-22.0750360128358,26.4155367732638,-40.5991777786305));
#22910=CARTESIAN_POINT('',(-26.7730012248527,23.5473502489538,-40.4353769712642));
#22911=CARTESIAN_POINT('Ctrl Pts',(-22.0750362323924,26.4155368863044,-40.843547806833));
#22912=CARTESIAN_POINT('Ctrl Pts',(-22.1513564730552,26.4548310187738,-40.837761028126));
#22913=CARTESIAN_POINT('Ctrl Pts',(-22.2292424792406,26.4910736721318,-40.8319373078903));
#22914=CARTESIAN_POINT('Ctrl Pts',(-22.4488693000598,26.5827774917964,-40.815847588764));
#22915=CARTESIAN_POINT('Ctrl Pts',(-22.5932160538874,26.6313795249419,-40.8056365593697));
#22916=CARTESIAN_POINT('Ctrl Pts',(-22.744709524646,26.6707071808935,-40.795616046995));
#22917=CARTESIAN_POINT('Ctrl Pts',(-22.7489520407912,26.6717993081585,-40.7953359836428));
#22918=CARTESIAN_POINT('Ctrl Pts',(-22.7581497491691,26.6741470360723,-40.7947300368079));
#22919=CARTESIAN_POINT('Ctrl Pts',(-22.763105740177,26.6753995077501,-40.794404305159));
#22920=CARTESIAN_POINT('Ctrl Pts',(-22.775744800319,26.6785616615831,-40.7935756028079));
#22921=CARTESIAN_POINT('Ctrl Pts',(-22.7834320173745,26.6804548478066,-40.7930734556238));
#22922=CARTESIAN_POINT('Ctrl Pts',(-22.7991796185297,26.6842716300435,-40.7920487361023));
#22923=CARTESIAN_POINT('Ctrl Pts',(-22.8072406164304,26.6861925067163,-40.791526308102));
#22924=CARTESIAN_POINT('Ctrl Pts',(-22.8236892354184,26.6900451075517,-40.7904647132452));
#22925=CARTESIAN_POINT('Ctrl Pts',(-22.8320773803821,26.6919743683588,-40.7899256835826));
#22926=CARTESIAN_POINT('Ctrl Pts',(-22.8435095494201,26.6945555718746,-40.7891943227393));
#22927=CARTESIAN_POINT('Ctrl Pts',(-22.8465468386675,26.695236720729,-40.7890003301954));
#22928=CARTESIAN_POINT('Ctrl Pts',(-22.8513502031162,26.6963066265373,-40.7886940406786));
#22929=CARTESIAN_POINT('Ctrl Pts',(-22.853115616823,26.6966982970831,-40.7885815752708));
#22930=CARTESIAN_POINT('Ctrl Pts',(-22.8565353884731,26.6974539801377,-40.7883639282661));
#22931=CARTESIAN_POINT('Ctrl Pts',(-22.8581896925598,26.6978181717698,-40.7882587370526));
#22932=CARTESIAN_POINT('Ctrl Pts',(-22.8621518649697,26.6986871611526,-40.7880070228545));
#22933=CARTESIAN_POINT('Ctrl Pts',(-22.8644600004047,26.6991907253768,-40.7878605719427));
#22934=CARTESIAN_POINT('Ctrl Pts',(-22.8692578584121,26.7002319451502,-40.7875565255609));
#22935=CARTESIAN_POINT('Ctrl Pts',(-22.87174767021,26.7007691882577,-40.7873989539083));
#22936=CARTESIAN_POINT('Ctrl Pts',(-22.8863910495771,26.7039107227969,-40.7864734503695));
#22937=CARTESIAN_POINT('Ctrl Pts',(-22.8985591876554,26.7064476858235,-40.7857093519794));
#22938=CARTESIAN_POINT('Ctrl Pts',(-22.9943078695785,26.7258332050058,-40.779733597182));
#22939=CARTESIAN_POINT('Ctrl Pts',(-23.078520773411,26.7394309678924,-40.774697527537));
#22940=CARTESIAN_POINT('Ctrl Pts',(-23.3050181855836,26.7668329683103,-40.7615003002726));
#22941=CARTESIAN_POINT('Ctrl Pts',(-23.4478478175809,26.7745428387671,-40.7535360495702));
#22942=CARTESIAN_POINT('Ctrl Pts',(-23.8548297887662,26.7694313910848,-40.730794007933));
#22943=CARTESIAN_POINT('Ctrl Pts',(-24.1174803372404,26.7336636119848,-40.7159687673348));
#22944=CARTESIAN_POINT('Ctrl Pts',(-24.38788742692,26.662282179612,-40.6990161378172));
#22945=CARTESIAN_POINT('Ctrl Pts',(-24.4029360095259,26.6581926245072,-40.6980673790172));
#22946=CARTESIAN_POINT('Ctrl Pts',(-24.4239099614613,26.6523290140556,-40.6967374069354));
#22947=CARTESIAN_POINT('Ctrl Pts',(-24.4298609693977,26.6506468295997,-40.696359187684));
#22948=CARTESIAN_POINT('Ctrl Pts',(-24.4390454245989,26.6480220679056,-40.6957741202273));
#22949=CARTESIAN_POINT('Ctrl Pts',(-24.4422823205954,26.6470915267879,-40.695567665271));
#22950=CARTESIAN_POINT('Ctrl Pts',(-24.4487303033242,26.6452269160755,-40.695155883721));
#22951=CARTESIAN_POINT('Ctrl Pts',(-24.4519414068243,26.6442929190231,-40.6949505597168));
#22952=CARTESIAN_POINT('Ctrl Pts',(-24.4590637188037,26.6422092597221,-40.694494574123));
#22953=CARTESIAN_POINT('Ctrl Pts',(-24.4629742065211,26.6410571722158,-40.6942438334242));
#22954=CARTESIAN_POINT('Ctrl Pts',(-24.4710348916886,26.6386657437119,-40.6937261873489));
#22955=CARTESIAN_POINT('Ctrl Pts',(-24.4751847958731,26.6374254502443,-40.6934592511492));
#22956=CARTESIAN_POINT('Ctrl Pts',(-24.4972610999111,26.6307789343835,-40.6920368970287));
#22957=CARTESIAN_POINT('Ctrl Pts',(-24.5151423338614,26.6252250180423,-40.6908766393347));
#22958=CARTESIAN_POINT('Ctrl Pts',(-24.5609105414444,26.6105708840475,-40.6878853850498));
#22959=CARTESIAN_POINT('Ctrl Pts',(-24.5887230219044,26.6012453175943,-40.6860470286971));
#22960=CARTESIAN_POINT('Ctrl Pts',(-24.6442329533307,26.5817858150694,-40.6823354778324));
#22961=CARTESIAN_POINT('Ctrl Pts',(-24.671926316966,26.5716487385447,-40.6804623271743));
#22962=CARTESIAN_POINT('Ctrl Pts',(-24.8259121274272,26.5128738771706,-40.6699249836441));
#22963=CARTESIAN_POINT('Ctrl Pts',(-24.9491682751369,26.4567039424799,-40.6610202831163));
#22964=CARTESIAN_POINT('Ctrl Pts',(-25.1592811798299,26.3444845037842,-40.6450703241916));
#22965=CARTESIAN_POINT('Ctrl Pts',(-25.2476685405325,26.2916906968821,-40.6381017438154));
#22966=CARTESIAN_POINT('Ctrl Pts',(-25.4946700202883,26.127625602962,-40.6180327134718));
#22967=CARTESIAN_POINT('Ctrl Pts',(-25.6460014370845,26.0061570290951,-40.6049666664731));
#22968=CARTESIAN_POINT('Ctrl Pts',(-25.7936628702886,25.8639844225203,-40.5920514785592));
#22969=CARTESIAN_POINT('Ctrl Pts',(-25.8017605601856,25.8561052625966,-40.5913427122474));
#22970=CARTESIAN_POINT('Ctrl Pts',(-25.8122944611703,25.8457472379028,-40.5904202560485));
#22971=CARTESIAN_POINT('Ctrl Pts',(-25.8147682054961,25.843306914023,-40.5902035965511));
#22972=CARTESIAN_POINT('Ctrl Pts',(-25.8185750417222,25.8395393402032,-40.5898701359819));
#22973=CARTESIAN_POINT('Ctrl Pts',(-25.819910916704,25.8382149257275,-40.5897531113613));
#22974=CARTESIAN_POINT('Ctrl Pts',(-25.8224369205943,25.8357062031361,-40.5895318151854));
#22975=CARTESIAN_POINT('Ctrl Pts',(-25.823627277617,25.8345221405837,-40.589427525368));
#22976=CARTESIAN_POINT('Ctrl Pts',(-25.826390214499,25.8317695149214,-40.5891854441443));
#22977=CARTESIAN_POINT('Ctrl Pts',(-25.827962095859,25.8302002585559,-40.5890477091122));
#22978=CARTESIAN_POINT('Ctrl Pts',(-25.8311939929272,25.8269670805934,-40.5887644905391));
#22979=CARTESIAN_POINT('Ctrl Pts',(-25.8328538138293,25.8253029648979,-40.5886190225669));
#22980=CARTESIAN_POINT('Ctrl Pts',(-25.8370952525269,25.8210412371743,-40.5882472588726));
#22981=CARTESIAN_POINT('Ctrl Pts',(-25.8396742744496,25.8184410289035,-40.5880211679012));
#22982=CARTESIAN_POINT('Ctrl Pts',(-25.874269672473,25.7834423134307,-40.5849877322549));
#22983=CARTESIAN_POINT('Ctrl Pts',(-25.9056021359536,25.7503709458318,-40.5822332859898));
#22984=CARTESIAN_POINT('Ctrl Pts',(-26.0028183027167,25.643301173013,-40.5736207399938));
#22985=CARTESIAN_POINT('Ctrl Pts',(-26.0660004207196,25.5669199209323,-40.5679216041295));
#22986=CARTESIAN_POINT('Ctrl Pts',(-26.1486623643995,25.4570455472252,-40.5601296995412));
#22987=CARTESIAN_POINT('Ctrl Pts',(-26.1712066981876,25.4259371027024,-40.5579661649992));
#22988=CARTESIAN_POINT('Ctrl Pts',(-26.2167651003378,25.3606462990484,-40.5534972349297));
#22989=CARTESIAN_POINT('Ctrl Pts',(-26.2396905324993,25.3264107902338,-40.5511933336223));
#22990=CARTESIAN_POINT('Ctrl Pts',(-26.4109220997595,25.05978385017,-40.5334843747185));
#22991=CARTESIAN_POINT('Ctrl Pts',(-26.5294909902898,24.8097077193418,-40.5180900092991));
#22992=CARTESIAN_POINT('Ctrl Pts',(-26.6203180774493,24.5306269804338,-40.5003147057651));
#22993=CARTESIAN_POINT('Ctrl Pts',(-26.6257036957868,24.5135991111972,-40.4992284949293));
#22994=CARTESIAN_POINT('Ctrl Pts',(-26.6326892756781,24.4908568446712,-40.497775261441));
#22995=CARTESIAN_POINT('Ctrl Pts',(-26.6344154573406,24.4851812998778,-40.4974123871669));
#22996=CARTESIAN_POINT('Ctrl Pts',(-26.6370824428728,24.4763247027596,-40.4968457951887));
#22997=CARTESIAN_POINT('Ctrl Pts',(-26.6380340284793,24.4731468888921,-40.4966424310991));
#22998=CARTESIAN_POINT('Ctrl Pts',(-26.6399277949692,24.466786952021,-40.4962352915862));
#22999=CARTESIAN_POINT('Ctrl Pts',(-26.6408699703951,24.4636048315246,-40.4960315162637));
#23000=CARTESIAN_POINT('Ctrl Pts',(-26.6429803550894,24.4564365236835,-40.4955723199325));
#23001=CARTESIAN_POINT('Ctrl Pts',(-26.6441457744967,24.4524495272685,-40.4953168080562));
#23002=CARTESIAN_POINT('Ctrl Pts',(-26.6465404396048,24.4441979726282,-40.4947877687786));
#23003=CARTESIAN_POINT('Ctrl Pts',(-26.6477685900406,24.4399331080866,-40.4945142061628));
#23004=CARTESIAN_POINT('Ctrl Pts',(-26.6509341031461,24.4288545659702,-40.493803259246));
#23005=CARTESIAN_POINT('Ctrl Pts',(-26.6528578096559,24.4220370406488,-40.4933654299952));
#23006=CARTESIAN_POINT('Ctrl Pts',(-26.6584373812404,24.4020109107513,-40.4920783450723));
#23007=CARTESIAN_POINT('Ctrl Pts',(-26.6620314498309,24.3887853876545,-40.4912270823696));
#23008=CARTESIAN_POINT('Ctrl Pts',(-26.6740925769035,24.3432570048757,-40.488292126506));
#23009=CARTESIAN_POINT('Ctrl Pts',(-26.6821416267725,24.3108465649558,-40.4861949952005));
#23010=CARTESIAN_POINT('Ctrl Pts',(-26.7452809481041,24.038588497622,-40.4685082034141));
#23011=CARTESIAN_POINT('Ctrl Pts',(-26.7732227470116,23.7933325710728,-40.452027638618));
#23012=CARTESIAN_POINT('Ctrl Pts',(-26.7730012248527,23.5473502489538,-40.4353769712642));
#23013=CARTESIAN_POINT('Ctrl Pts',(-26.7730012238456,23.5473491308651,-40.4353768955802));
#23014=CARTESIAN_POINT('Ctrl Pts',(-26.7728090040715,23.33398691809,-40.4209342997964));
#23015=CARTESIAN_POINT('Ctrl Pts',(-26.7514288037154,23.1211364370925,-40.4064672452439));
#23016=CARTESIAN_POINT('Ctrl Pts',(-26.7080768764898,22.9065968620062,-40.3927228443158));
#23017=CARTESIAN_POINT('Ctrl Pts',(-26.706984812474,22.901262144858,-40.3923816401998));
#23018=CARTESIAN_POINT('Ctrl Pts',(-26.705252840185,22.8929092925769,-40.3918483080951));
#23019=CARTESIAN_POINT('Ctrl Pts',(-26.7046221164231,22.8898892955003,-40.3916556668281));
#23020=CARTESIAN_POINT('Ctrl Pts',(-26.7035529623943,22.8848065132523,-40.3913317628625));
#23021=CARTESIAN_POINT('Ctrl Pts',(-26.7031168439663,22.8827432522273,-40.3912003687335));
#23022=CARTESIAN_POINT('Ctrl Pts',(-26.7022526773045,22.8786746515126,-40.3909414460159));
#23023=CARTESIAN_POINT('Ctrl Pts',(-26.7018247398349,22.8766692896164,-40.3908139111171));
#23024=CARTESIAN_POINT('Ctrl Pts',(-26.7009993821942,22.8728195784806,-40.390569245984));
#23025=CARTESIAN_POINT('Ctrl Pts',(-26.7006022575248,22.8709751752274,-40.3904520993814));
#23026=CARTESIAN_POINT('Ctrl Pts',(-26.6996851997146,22.8667341000169,-40.3901828949823));
#23027=CARTESIAN_POINT('Ctrl Pts',(-26.6991641490948,22.8643376661808,-40.390030901957));
#23028=CARTESIAN_POINT('Ctrl Pts',(-26.6975012763788,22.8567315543887,-40.3895488669505));
#23029=CARTESIAN_POINT('Ctrl Pts',(-26.696349249691,22.8515240802496,-40.3892194112805));
#23030=CARTESIAN_POINT('Ctrl Pts',(-26.6864089187849,22.8071140887442,-40.3864144214184));
#23031=CARTESIAN_POINT('Ctrl Pts',(-26.6769007028632,22.7680740306628,-40.3839795347652));
#23032=CARTESIAN_POINT('Ctrl Pts',(-26.6649277605561,22.722628070755,-40.3811705483139));
#23033=CARTESIAN_POINT('Ctrl Pts',(-26.6631702085471,22.7160417859539,-40.3807640830489));
#23034=CARTESIAN_POINT('Ctrl Pts',(-26.6609689012003,22.707896396793,-40.3802621224018));
#23035=CARTESIAN_POINT('Ctrl Pts',(-26.6605448633145,22.7063320369776,-40.3801657515795));
#23036=CARTESIAN_POINT('Ctrl Pts',(-26.6593613663262,22.7019788901117,-40.3798976706361));
#23037=CARTESIAN_POINT('Ctrl Pts',(-26.6585993336444,22.6991907974415,-40.3797260740336));
#23038=CARTESIAN_POINT('Ctrl Pts',(-26.6526237517894,22.6774426793,-40.3783883380882));
#23039=CARTESIAN_POINT('Ctrl Pts',(-26.6472404150811,22.6585293074089,-40.3772295888355));
#23040=CARTESIAN_POINT('Ctrl Pts',(-26.6296783214793,22.5989061852302,-40.3735879415328));
#23041=CARTESIAN_POINT('Ctrl Pts',(-26.6168670621754,22.5583862854609,-40.3711296870645));
#23042=CARTESIAN_POINT('Ctrl Pts',(-26.5716482755289,22.4246296693829,-40.3630350486516));
#23043=CARTESIAN_POINT('Ctrl Pts',(-26.5357587975781,22.3326265459007,-40.3574989022638));
#23044=CARTESIAN_POINT('Ctrl Pts',(-26.4841783225591,22.2164596865587,-40.3503908882467));
#23045=CARTESIAN_POINT('Ctrl Pts',(-26.4723122462374,22.1906603395344,-40.348804659764));
#23046=CARTESIAN_POINT('Ctrl Pts',(-26.4497429699397,22.1432507117845,-40.3458706615062));
#23047=CARTESIAN_POINT('Ctrl Pts',(-26.4391352160234,22.1215973059098,-40.3445231247795));
#23048=CARTESIAN_POINT('Ctrl Pts',(-26.4061624347003,22.0561597323288,-40.3404232162477));
#23049=CARTESIAN_POINT('Ctrl Pts',(-26.3830378614903,22.0127669787064,-40.3376664425618));
#23050=CARTESIAN_POINT('Ctrl Pts',(-26.2898167477981,21.8470878184802,-40.3269452703998));
#23051=CARTESIAN_POINT('Ctrl Pts',(-26.2127272691422,21.7289331720181,-40.3188703249029));
#23052=CARTESIAN_POINT('Ctrl Pts',(-26.0948272382408,21.5717829548074,-40.3072157363963));
#23053=CARTESIAN_POINT('Ctrl Pts',(-26.0603549912444,21.5282269700936,-40.3038799579491));
#23054=CARTESIAN_POINT('Ctrl Pts',(-26.0203627061881,21.4802958303968,-40.3000792748139));
#23055=CARTESIAN_POINT('Ctrl Pts',(-26.0159323870267,21.4750205279814,-40.2996591599074));
#23056=CARTESIAN_POINT('Ctrl Pts',(-26.0086730255115,21.4664326704055,-40.2989722551929));
#23057=CARTESIAN_POINT('Ctrl Pts',(-26.0058541049344,21.4631115561181,-40.2987058809369));
#23058=CARTESIAN_POINT('Ctrl Pts',(-26.0003724684329,21.4566798379406,-40.2981885867273));
#23059=CARTESIAN_POINT('Ctrl Pts',(-25.9977105396042,21.4535685717934,-40.2979376995041));
#23060=CARTESIAN_POINT('Ctrl Pts',(-25.9930728243981,21.4481688700075,-40.2975011368674));
#23061=CARTESIAN_POINT('Ctrl Pts',(-25.9910997292911,21.4458781208396,-40.2973155731066));
#23062=CARTESIAN_POINT('Ctrl Pts',(-25.9869819964881,21.4411110453085,-40.2969286639918));
#23063=CARTESIAN_POINT('Ctrl Pts',(-25.9848368015399,21.4386352067335,-40.2967272955936));
#23064=CARTESIAN_POINT('Ctrl Pts',(-25.9795821933868,21.43258934533,-40.2962345280942));
#23065=CARTESIAN_POINT('Ctrl Pts',(-25.9764686879894,21.4290229027711,-40.2959429585393));
#23066=CARTESIAN_POINT('Ctrl Pts',(-25.9645421633474,21.415421976963,-40.2948276264822));
#23067=CARTESIAN_POINT('Ctrl Pts',(-25.9556747546757,21.4054355596711,-40.294001588334));
#23068=CARTESIAN_POINT('Ctrl Pts',(-25.9438943778807,21.3923335201162,-40.2929083217936));
#23069=CARTESIAN_POINT('Ctrl Pts',(-25.941036839078,21.3891680484706,-40.29264344752));
#23070=CARTESIAN_POINT('Ctrl Pts',(-25.7604561116888,21.1899241694814,-40.2759246704034));
#23071=CARTESIAN_POINT('Ctrl Pts',(-25.5593040574696,21.0165196869184,-40.2583799044899));
#23072=CARTESIAN_POINT('Ctrl Pts',(-25.276053420008,20.8274768284793,-40.2353463814289));
#23073=CARTESIAN_POINT('Ctrl Pts',(-25.2113509371624,20.7875277079221,-40.2301926783903));
#23074=CARTESIAN_POINT('Ctrl Pts',(-25.0715661907385,20.7079080676913,-40.2193464386802));
#23075=CARTESIAN_POINT('Ctrl Pts',(-24.9962021987853,20.6688382172622,-40.2136647681925));
#23076=CARTESIAN_POINT('Ctrl Pts',(-24.8719456507937,20.6105262815491,-40.2046484729325));
#23077=CARTESIAN_POINT('Ctrl Pts',(-24.8239721592532,20.5894245851671,-40.201248924994));
#23078=CARTESIAN_POINT('Ctrl Pts',(-24.7601364639828,20.5631846643062,-40.1968509746676));
#23079=CARTESIAN_POINT('Ctrl Pts',(-24.7447214051119,20.5569871389449,-40.1957984551897));
#23080=CARTESIAN_POINT('Ctrl Pts',(-24.7195310323174,20.5470851037085,-40.1940947209419));
#23081=CARTESIAN_POINT('Ctrl Pts',(-24.709784621622,20.5433085428342,-40.1934394599967));
#23082=CARTESIAN_POINT('Ctrl Pts',(-24.6977599725807,20.5387163643039,-40.1926360161078));
#23083=CARTESIAN_POINT('Ctrl Pts',(-24.6954991143757,20.5378558646967,-40.1924851701086));
#23084=CARTESIAN_POINT('Ctrl Pts',(-24.6911145042708,20.5361926987496,-40.1921930483267));
#23085=CARTESIAN_POINT('Ctrl Pts',(-24.6889908697662,20.5353897297539,-40.1920517544081));
#23086=CARTESIAN_POINT('Ctrl Pts',(-24.685138638256,20.5339378105854,-40.1917958000539));
#23087=CARTESIAN_POINT('Ctrl Pts',(-24.68341033856,20.5332881042552,-40.1916810942011));
#23088=CARTESIAN_POINT('Ctrl Pts',(-24.6799054108221,20.5319739605548,-40.1914487340515));
#23089=CARTESIAN_POINT('Ctrl Pts',(-24.678128761504,20.5313096089814,-40.1913310851819));
#23090=CARTESIAN_POINT('Ctrl Pts',(-24.6730228846216,20.5294054786565,-40.1909933601625));
#23091=CARTESIAN_POINT('Ctrl Pts',(-24.6696921788465,20.528169630791,-40.1907735210759));
#23092=CARTESIAN_POINT('Ctrl Pts',(-24.6551442317445,20.5227990116683,-40.1898153169774));
#23093=CARTESIAN_POINT('Ctrl Pts',(-24.6439058878432,20.5187210982591,-40.1890803249247));
#23094=CARTESIAN_POINT('Ctrl Pts',(-24.4500431854462,20.4495949983909,-40.1764871510084));
#23095=CARTESIAN_POINT('Ctrl Pts',(-24.2619072617459,20.4010824404704,-40.1655576380878));
#23096=CARTESIAN_POINT('Ctrl Pts',(-23.9194117925328,20.3450559118602,-40.1461324522901));
#23097=CARTESIAN_POINT('Ctrl Pts',(-23.76673065637,20.3311378554512,-40.1376331373063));
#23098=CARTESIAN_POINT('Ctrl Pts',(-23.5883020509026,20.3276274723848,-40.1274528576264));
#23099=CARTESIAN_POINT('Ctrl Pts',(-23.5629552083704,20.3274278941249,-40.1260011891407));
#23100=CARTESIAN_POINT('Ctrl Pts',(-23.4210353583722,20.327984679949,-40.1178350533521));
#23101=CARTESIAN_POINT('Ctrl Pts',(-23.304584291837,20.3347666136513,-40.1109861129622));
#23102=CARTESIAN_POINT('Ctrl Pts',(-23.1693525475861,20.350031537355,-40.1027503946933));
#23103=CARTESIAN_POINT('Ctrl Pts',(-23.1499606870289,20.3523992480943,-40.1015627158175));
#23104=CARTESIAN_POINT('Ctrl Pts',(-23.1262431227944,20.3555142291803,-40.1001015446441));
#23105=CARTESIAN_POINT('Ctrl Pts',(-23.1218955551241,20.3560942543528,-40.0998333508604));
#23106=CARTESIAN_POINT('Ctrl Pts',(-23.1134702466269,20.357235816851,-40.0993129191522));
#23107=CARTESIAN_POINT('Ctrl Pts',(-23.1093923689749,20.357796295112,-40.0990607151952));
#23108=CARTESIAN_POINT('Ctrl Pts',(-23.1023187221247,20.3587823343579,-40.09862268464));
#23109=CARTESIAN_POINT('Ctrl Pts',(-23.099322450921,20.3592043057354,-40.0984369720671));
#23110=CARTESIAN_POINT('Ctrl Pts',(-23.0930937173308,20.3600904597528,-40.0980505508678));
#23111=CARTESIAN_POINT('Ctrl Pts',(-23.0898613585859,20.3605553369116,-40.097849820402));
#23112=CARTESIAN_POINT('Ctrl Pts',(-23.0810139460352,20.3618414986518,-40.0972998432591));
#23113=CARTESIAN_POINT('Ctrl Pts',(-23.0754003658151,20.3626726996274,-40.0969502822247));
#23114=CARTESIAN_POINT('Ctrl Pts',(-23.0539459556236,20.3659073786006,-40.0956119611507));
#23115=CARTESIAN_POINT('Ctrl Pts',(-23.038121141403,20.3684141172482,-40.0946199265348));
#23116=CARTESIAN_POINT('Ctrl Pts',(-22.7773741527612,20.4117134654495,-40.0781916151624));
#23117=CARTESIAN_POINT('Ctrl Pts',(-22.5380074425618,20.4805492046857,-40.061808441389));
#23118=CARTESIAN_POINT('Ctrl Pts',(-22.1602701591182,20.6382039929131,-40.0341642434919));
#23119=CARTESIAN_POINT('Ctrl Pts',(-22.0164392940135,20.7113270832848,-40.0231871039986));
#23120=CARTESIAN_POINT('Ctrl Pts',(-21.8225074920731,20.8289787688683,-40.0081780160742));
#23121=CARTESIAN_POINT('Ctrl Pts',(-21.7673884618637,20.864767325848,-40.0038885083397));
#23122=CARTESIAN_POINT('Ctrl Pts',(-21.6900635048681,20.9184051065155,-39.9978773981317));
#23123=CARTESIAN_POINT('Ctrl Pts',(-21.6669426234804,20.9349001632806,-39.9960809289446));
#23124=CARTESIAN_POINT('Ctrl Pts',(-21.6404687670021,20.9543204887099,-39.9940278510597));
#23125=CARTESIAN_POINT('Ctrl Pts',(-21.6369010570518,20.9569489754713,-39.9937512544272));
#23126=CARTESIAN_POINT('Ctrl Pts',(-21.6314758351121,20.9609632620887,-39.9933307906694));
#23127=CARTESIAN_POINT('Ctrl Pts',(-21.6296143959316,20.9623437070684,-39.9931865515019));
#23128=CARTESIAN_POINT('Ctrl Pts',(-21.6262564594201,20.96483957435,-39.9929264002738));
#23129=CARTESIAN_POINT('Ctrl Pts',(-21.624759445966,20.9659542859416,-39.9928104389379));
#23130=CARTESIAN_POINT('Ctrl Pts',(-21.621761414811,20.9681907419793,-39.9925782416574));
#23131=CARTESIAN_POINT('Ctrl Pts',(-21.620260413109,20.9693124905376,-39.9924620068526));
#23132=CARTESIAN_POINT('Ctrl Pts',(-21.6160076320632,20.9724965199665,-39.9921327267443));
#23133=CARTESIAN_POINT('Ctrl Pts',(-21.6132581633257,20.9745619049072,-39.9919198999694));
#23134=CARTESIAN_POINT('Ctrl Pts',(-21.6017248823035,20.9832545501021,-39.99102736134));
#23135=CARTESIAN_POINT('Ctrl Pts',(-21.5929716003735,20.9899224744371,-39.9903504799354));
#23136=CARTESIAN_POINT('Ctrl Pts',(-21.4466027048217,21.1026101713468,-39.9790374519262));
#23137=CARTESIAN_POINT('Ctrl Pts',(-21.3177243421066,21.2195590048627,-39.9691515165728));
#23138=CARTESIAN_POINT('Ctrl Pts',(-21.0556571676399,21.49916037971,-39.9476349681803));
#23139=CARTESIAN_POINT('Ctrl Pts',(-20.9276705892199,21.6655653903238,-39.9360912263759));
#23140=CARTESIAN_POINT('Ctrl Pts',(-20.7733354955943,21.9127048323666,-39.9192658599859));
#23141=CARTESIAN_POINT('Ctrl Pts',(-20.7326053494256,21.9838255614106,-39.9144619955773));
#23142=CARTESIAN_POINT('Ctrl Pts',(-20.6754939923929,22.0929998259467,-39.9070929794505));
#23143=CARTESIAN_POINT('Ctrl Pts',(-20.6570621736822,22.1299457272625,-39.904600285239));
#23144=CARTESIAN_POINT('Ctrl Pts',(-20.636053319676,22.1741640976276,-39.9016146378716));
#23145=CARTESIAN_POINT('Ctrl Pts',(-20.6327856184943,22.1811056314392,-39.9011458783804));
#23146=CARTESIAN_POINT('Ctrl Pts',(-20.6278041554539,22.1917864961383,-39.900424481549));
#23147=CARTESIAN_POINT('Ctrl Pts',(-20.6260726979322,22.1955175830353,-39.9001724573281));
#23148=CARTESIAN_POINT('Ctrl Pts',(-20.6230800834447,22.2019987817099,-39.8997346276199));
#23149=CARTESIAN_POINT('Ctrl Pts',(-20.6218156444841,22.2047473798406,-39.8995489358337));
#23150=CARTESIAN_POINT('Ctrl Pts',(-20.6191938874503,22.2104676758951,-39.8991624500491));
#23151=CARTESIAN_POINT('Ctrl Pts',(-20.617837214419,22.2134396641982,-39.8989616340473));
#23152=CARTESIAN_POINT('Ctrl Pts',(-20.6145389230538,22.2206942287483,-39.8984714027439));
#23153=CARTESIAN_POINT('Ctrl Pts',(-20.6126021579517,22.2249789923167,-39.8981818205634));
#23154=CARTESIAN_POINT('Ctrl Pts',(-20.6052884030514,22.2412542400645,-39.8970817200948));
#23155=CARTESIAN_POINT('Ctrl Pts',(-20.5999754486934,22.253273205806,-39.8962690045195));
#23156=CARTESIAN_POINT('Ctrl Pts',(-20.509508474693,22.4613599985542,-39.8821918755898));
#23157=CARTESIAN_POINT('Ctrl Pts',(-20.444013136071,22.6653483051592,-39.8682386522577));
#23158=CARTESIAN_POINT('Ctrl Pts',(-20.3618525863434,23.0483411039515,-39.8419403043687));
#23159=CARTESIAN_POINT('Ctrl Pts',(-20.3389996104594,23.2251937547888,-39.8297744148685));
#23160=CARTESIAN_POINT('Ctrl Pts',(-20.3270334938343,23.4868580572614,-39.8123081553058));
#23161=CARTESIAN_POINT('Ctrl Pts',(-20.3264753292174,23.57081386154,-39.8067883555873));
#23162=CARTESIAN_POINT('Ctrl Pts',(-20.3302133716348,23.6860889507761,-39.7994054389666));
#23163=CARTESIAN_POINT('Ctrl Pts',(-20.3316899070629,23.7174606032992,-39.7974162820961));
#23164=CARTESIAN_POINT('Ctrl Pts',(-20.3339046919158,23.753340609348,-39.795168075968));
#23165=CARTESIAN_POINT('Ctrl Pts',(-20.334194121901,23.7578735786363,-39.794884535014));
#23166=CARTESIAN_POINT('Ctrl Pts',(-20.3346472320892,23.7647416900706,-39.794455687903));
#23167=CARTESIAN_POINT('Ctrl Pts',(-20.3348038730589,23.7670772666142,-39.7943099867682));
#23168=CARTESIAN_POINT('Ctrl Pts',(-20.3350780525419,23.7710997424826,-39.794059282733));
#23169=CARTESIAN_POINT('Ctrl Pts',(-20.3351943739232,23.7727867180712,-39.7939542108686));
#23170=CARTESIAN_POINT('Ctrl Pts',(-20.335438465745,23.7762865704525,-39.7937363717669));
#23171=CARTESIAN_POINT('Ctrl Pts',(-20.3355664415592,23.7780994259754,-39.7936236165767));
#23172=CARTESIAN_POINT('Ctrl Pts',(-20.3359209985551,23.7830621764835,-39.7933151656401));
#23173=CARTESIAN_POINT('Ctrl Pts',(-20.3361506770967,23.786211858943,-39.7931196454302));
#23174=CARTESIAN_POINT('Ctrl Pts',(-20.3370462209025,23.7982488922111,-39.7923733429715));
#23175=CARTESIAN_POINT('Ctrl Pts',(-20.3377443291862,23.8071339124758,-39.7918243642188));
#23176=CARTESIAN_POINT('Ctrl Pts',(-20.3499378417435,23.9544934827857,-39.7827492537357));
#23177=CARTESIAN_POINT('Ctrl Pts',(-20.370341955992,24.0921052883501,-39.7747088752091));
#23178=CARTESIAN_POINT('Ctrl Pts',(-20.4461861410096,24.4446931552396,-39.754268003905));
#23179=CARTESIAN_POINT('Ctrl Pts',(-20.5150332037432,24.656009666628,-39.742138835494));
#23180=CARTESIAN_POINT('Ctrl Pts',(-20.6580060693181,24.9778588574961,-39.7219850162191));
#23181=CARTESIAN_POINT('Ctrl Pts',(-20.718177191576,25.0937850009049,-39.7143531401263));
#23182=CARTESIAN_POINT('Ctrl Pts',(-20.7959372328057,25.2236626301882,-39.7051996612479));
#23183=CARTESIAN_POINT('Ctrl Pts',(-20.8068441001825,25.2414841152972,-39.7039300224255));
#23184=CARTESIAN_POINT('Ctrl Pts',(-20.8211630680579,25.2643778448708,-39.7022808678945));
#23185=CARTESIAN_POINT('Ctrl Pts',(-20.8244175488238,25.2695484733955,-39.7019071922724));
#23186=CARTESIAN_POINT('Ctrl Pts',(-20.8296801696184,25.277857076888,-39.7013047775619));
#23187=CARTESIAN_POINT('Ctrl Pts',(-20.8316790930147,25.2810008958957,-39.7010763813924));
#23188=CARTESIAN_POINT('Ctrl Pts',(-20.8354931096982,25.2869765042359,-39.7006413901369));
#23189=CARTESIAN_POINT('Ctrl Pts',(-20.837307194958,25.2898089337294,-39.700434832831));
#23190=CARTESIAN_POINT('Ctrl Pts',(-20.8414480063552,25.2962519750551,-39.6999641177813));
#23191=CARTESIAN_POINT('Ctrl Pts',(-20.8437775198776,25.299860780086,-39.6996998560868));
#23192=CARTESIAN_POINT('Ctrl Pts',(-20.8508842577332,25.3108221458232,-39.6988953241589));
#23193=CARTESIAN_POINT('Ctrl Pts',(-20.8556842507498,25.3181598317395,-39.6983542011337));
#23194=CARTESIAN_POINT('Ctrl Pts',(-20.8900549062457,25.3702366447541,-39.6944953684415));
#23195=CARTESIAN_POINT('Ctrl Pts',(-20.9207067849185,25.4142488256529,-39.6911369679976));
#23196=CARTESIAN_POINT('Ctrl Pts',(-20.9589469199173,25.466335422606,-39.6870400413801));
#23197=CARTESIAN_POINT('Ctrl Pts',(-20.9654980726549,25.4751636465597,-39.6863413099574));
#23198=CARTESIAN_POINT('Ctrl Pts',(-21.0113117009467,25.5362457419083,-39.6814765026779));
#23199=CARTESIAN_POINT('Ctrl Pts',(-21.0521084289258,25.5873251053595,-39.6772529959035));
#23200=CARTESIAN_POINT('Ctrl Pts',(-21.2251427188022,25.7909511895672,-39.6597711194017));
#23201=CARTESIAN_POINT('Ctrl Pts',(-21.3700103895921,25.9321413639984,-39.646068561947));
#23202=CARTESIAN_POINT('Ctrl Pts',(-21.6623120715856,26.1678788641579,-39.6206869424311));
#23203=CARTESIAN_POINT('Ctrl Pts',(-21.8061276032853,26.2658245013485,-39.6090450385963));
#23204=CARTESIAN_POINT('Ctrl Pts',(-21.9663039778016,26.3569116342803,-39.5974455962901));
#23205=CARTESIAN_POINT('Ctrl Pts',(-21.9754787399383,26.3620697113195,-39.5967857451467));
#23206=CARTESIAN_POINT('Ctrl Pts',(-21.9875110948863,26.3687569691971,-39.5959264823079));
#23207=CARTESIAN_POINT('Ctrl Pts',(-21.9903458194818,26.3703268413455,-39.5957244883641));
#23208=CARTESIAN_POINT('Ctrl Pts',(-21.9949796181568,26.3728839171312,-39.5953950241984));
#23209=CARTESIAN_POINT('Ctrl Pts',(-21.9967772670928,26.3738736776636,-39.595267389153));
#23210=CARTESIAN_POINT('Ctrl Pts',(-22.0002289989648,26.3757698592013,-39.5950226560652));
#23211=CARTESIAN_POINT('Ctrl Pts',(-22.001882927348,26.3766765424203,-39.5949055414335));
#23212=CARTESIAN_POINT('Ctrl Pts',(-22.0056861693659,26.3787571388064,-39.5946365801415));
#23213=CARTESIAN_POINT('Ctrl Pts',(-22.0078360309838,26.3799300572301,-39.5944847978675));
#23214=CARTESIAN_POINT('Ctrl Pts',(-22.0146560710465,26.3836408431977,-39.5940040936381));
#23215=CARTESIAN_POINT('Ctrl Pts',(-22.0193312229294,26.386169625166,-39.5936757534056));
#23216=CARTESIAN_POINT('Ctrl Pts',(-22.0409399380988,26.3977887359841,-39.5921635094053));
#23217=CARTESIAN_POINT('Ctrl Pts',(-22.0579484072219,26.4067390708759,-39.5909883551281));
#23218=CARTESIAN_POINT('Ctrl Pts',(-22.0750360153868,26.4155367745772,-39.5898217886697));
#23219=CARTESIAN_POINT('Origin',(-23.5502525316942,23.5502525316942,-77.3107734492734));
#23220=CARTESIAN_POINT('',(-22.0750360152969,26.415536774531,-38.0939694478973));
#23221=CARTESIAN_POINT('',(-22.0750360565132,26.4155367957515,-38.344122456765));
#23222=CARTESIAN_POINT('',(-22.0750360153461,26.4155367745563,-77.3107734492734));
#23223=CARTESIAN_POINT('',(-26.7730017872581,23.5524430253128,-38.936921602977));
#23224=CARTESIAN_POINT('Ctrl Pts',(-22.0750360152969,26.415536774531,-38.0939694478973));
#23225=CARTESIAN_POINT('Ctrl Pts',(-22.0709270299416,26.4134212276783,-38.0942379738773));
#23226=CARTESIAN_POINT('Ctrl Pts',(-22.0668223643516,26.4112967231257,-38.0945067643071));
#23227=CARTESIAN_POINT('Ctrl Pts',(-21.9751324508798,26.3635892031279,-38.1005233920934));
#23228=CARTESIAN_POINT('Ctrl Pts',(-21.8896913901989,26.3140181099801,-38.1063855786955));
#23229=CARTESIAN_POINT('Ctrl Pts',(-21.7988048027281,26.2555502581609,-38.1129634702086));
#23230=CARTESIAN_POINT('Ctrl Pts',(-21.7909656919704,26.2504589587677,-38.1135336850914));
#23231=CARTESIAN_POINT('Ctrl Pts',(-21.7793647659388,26.2428524944705,-38.1143818353013));
#23232=CARTESIAN_POINT('Ctrl Pts',(-21.7755858711397,26.2403633625005,-38.1146587936373));
#23233=CARTESIAN_POINT('Ctrl Pts',(-21.7691282865532,26.236090267628,-38.1151332480238));
#23234=CARTESIAN_POINT('Ctrl Pts',(-21.7664469959437,26.2343102305726,-38.1153305960743));
#23235=CARTESIAN_POINT('Ctrl Pts',(-21.7610128888376,26.2306909331183,-38.1157312637284));
#23236=CARTESIAN_POINT('Ctrl Pts',(-21.7582602320776,26.2288514418309,-38.11593459187));
#23237=CARTESIAN_POINT('Ctrl Pts',(-21.7519572955152,26.2246253752415,-38.1164010152609));
#23238=CARTESIAN_POINT('Ctrl Pts',(-21.7484089290834,26.2222359699319,-38.1166642174274));
#23239=CARTESIAN_POINT('Ctrl Pts',(-21.7409779281124,26.2172105356521,-38.1172167223357));
#23240=CARTESIAN_POINT('Ctrl Pts',(-21.7370962756336,26.2145730786207,-38.1175060789575));
#23241=CARTESIAN_POINT('Ctrl Pts',(-21.7268678973606,26.2075905227487,-38.1182705417728));
#23242=CARTESIAN_POINT('Ctrl Pts',(-21.7205309707127,26.2032311842765,-38.1187461900505));
#23243=CARTESIAN_POINT('Ctrl Pts',(-21.7016081185116,26.1901136091846,-38.1201726637776));
#23244=CARTESIAN_POINT('Ctrl Pts',(-21.6890691669111,26.1812882867504,-38.1211260535671));
#23245=CARTESIAN_POINT('Ctrl Pts',(-21.5489092520977,26.0811358525208,-38.1318760480398));
#23246=CARTESIAN_POINT('Ctrl Pts',(-21.4280791115379,25.98070765852,-38.1420314087641));
#23247=CARTESIAN_POINT('Ctrl Pts',(-21.0821440450911,25.647653310951,-38.1739234167877));
#23248=CARTESIAN_POINT('Ctrl Pts',(-20.8843151276914,25.389659725045,-38.1965121002003));
#23249=CARTESIAN_POINT('Ctrl Pts',(-20.7205405263816,25.0926851585918,-38.2179697241785));
#23250=CARTESIAN_POINT('Ctrl Pts',(-20.7129937831087,25.0787587500689,-38.2189659817496));
#23251=CARTESIAN_POINT('Ctrl Pts',(-20.7038549265296,25.0615934076616,-38.2201812071793));
#23252=CARTESIAN_POINT('Ctrl Pts',(-20.7021653481048,25.0584070214745,-38.2204062525793));
#23253=CARTESIAN_POINT('Ctrl Pts',(-20.6993923305966,25.0531560922515,-38.2207762210184));
#23254=CARTESIAN_POINT('Ctrl Pts',(-20.6983057828304,25.0510932095327,-38.2209213413679));
#23255=CARTESIAN_POINT('Ctrl Pts',(-20.6963530149324,25.0473759728002,-38.221182434114));
#23256=CARTESIAN_POINT('Ctrl Pts',(-20.6954859960088,25.0457220487599,-38.2212984574647));
#23257=CARTESIAN_POINT('Ctrl Pts',(-20.6936272148162,25.0421687333229,-38.221547410831));
#23258=CARTESIAN_POINT('Ctrl Pts',(-20.6926359118676,25.0402691114227,-38.2216803111981));
#23259=CARTESIAN_POINT('Ctrl Pts',(-20.6899324047292,25.0350757918172,-38.2220431245093));
#23260=CARTESIAN_POINT('Ctrl Pts',(-20.6882239888641,25.0317801091894,-38.2222727961594));
#23261=CARTESIAN_POINT('Ctrl Pts',(-20.6794656054694,25.0148127397329,-38.2234523385782));
#23262=CARTESIAN_POINT('Ctrl Pts',(-20.6725077366294,25.0010933553143,-38.2243964462812));
#23263=CARTESIAN_POINT('Ctrl Pts',(-20.6077230931501,24.8710524904951,-38.233259516684));
#23264=CARTESIAN_POINT('Ctrl Pts',(-20.5568732369388,24.7513691183257,-38.2407732282274));
#23265=CARTESIAN_POINT('Ctrl Pts',(-20.3953358254907,24.2965819194516,-38.2681403222025));
#23266=CARTESIAN_POINT('Ctrl Pts',(-20.3326472514567,23.9471472591325,-38.2871754025));
#23267=CARTESIAN_POINT('Ctrl Pts',(-20.3275065378465,23.572663417507,-38.3098055194338));
#23268=CARTESIAN_POINT('Ctrl Pts',(-20.3274286749555,23.5508362351364,-38.3111311815913));
#23269=CARTESIAN_POINT('Ctrl Pts',(-20.3276148685454,23.522588549216,-38.3128559052357));
#23270=CARTESIAN_POINT('Ctrl Pts',(-20.3276763923069,23.5161669221205,-38.3132486008971));
#23271=CARTESIAN_POINT('Ctrl Pts',(-20.3278048123216,23.5059505846615,-38.3138743347191));
#23272=CARTESIAN_POINT('Ctrl Pts',(-20.327859218912,23.5021557112028,-38.3141069804427));
#23273=CARTESIAN_POINT('Ctrl Pts',(-20.3279735285888,23.4950573769451,-38.3145425530568));
#23274=CARTESIAN_POINT('Ctrl Pts',(-20.3280318086554,23.4917538919533,-38.3147454287036));
#23275=CARTESIAN_POINT('Ctrl Pts',(-20.3281732709396,23.4843785060941,-38.3151987414645));
#23276=CARTESIAN_POINT('Ctrl Pts',(-20.3282590919795,23.4803066667307,-38.315449261137));
#23277=CARTESIAN_POINT('Ctrl Pts',(-20.3285314820217,23.4684498320328,-38.316179493546));
#23278=CARTESIAN_POINT('Ctrl Pts',(-20.3287385485403,23.4606653774087,-38.3166598492434));
#23279=CARTESIAN_POINT('Ctrl Pts',(-20.3292700634214,23.4430814729808,-38.3177470334374));
#23280=CARTESIAN_POINT('Ctrl Pts',(-20.3296110216558,23.433282633241,-38.3183543771412));
#23281=CARTESIAN_POINT('Ctrl Pts',(-20.3308341740776,23.4022109387528,-38.3202850638725));
#23282=CARTESIAN_POINT('Ctrl Pts',(-20.3318824503267,23.3809455358753,-38.3216136033708));
#23283=CARTESIAN_POINT('Ctrl Pts',(-20.3370068048824,23.2944341255461,-38.3270483924466));
#23284=CARTESIAN_POINT('Ctrl Pts',(-20.3428567434016,23.2293126301799,-38.3312095247524));
#23285=CARTESIAN_POINT('Ctrl Pts',(-20.3706662053572,22.9987001952099,-38.3462014970982));
#23286=CARTESIAN_POINT('Ctrl Pts',(-20.4034919239815,22.8348054631395,-38.357345225422));
#23287=CARTESIAN_POINT('Ctrl Pts',(-20.4859755520085,22.5427945099748,-38.3778456214333));
#23288=CARTESIAN_POINT('Ctrl Pts',(-20.5314112047669,22.4138707363317,-38.3871335951902));
#23289=CARTESIAN_POINT('Ctrl Pts',(-20.601209406924,22.2498683139141,-38.3990180872388));
#23290=CARTESIAN_POINT('Ctrl Pts',(-20.6182728260268,22.2118393960573,-38.4017783108198));
#23291=CARTESIAN_POINT('Ctrl Pts',(-20.6455219816844,22.1541336146427,-38.4059630508232));
#23292=CARTESIAN_POINT('Ctrl Pts',(-20.6551805242275,22.1342137896937,-38.4074069142896));
#23293=CARTESIAN_POINT('Ctrl Pts',(-20.6871831537003,22.0699077998681,-38.4120622380886));
#23294=CARTESIAN_POINT('Ctrl Pts',(-20.7103500417138,22.0259358591252,-38.4152364884836));
#23295=CARTESIAN_POINT('Ctrl Pts',(-20.7372414254265,21.9776377559863,-38.4186983803039));
#23296=CARTESIAN_POINT('Ctrl Pts',(-20.7399693380059,21.972768113658,-38.4190471406211));
#23297=CARTESIAN_POINT('Ctrl Pts',(-20.7438446490465,21.9658921876036,-38.4195391605764));
#23298=CARTESIAN_POINT('Ctrl Pts',(-20.7449815554936,21.9638800489896,-38.4196830908934));
#23299=CARTESIAN_POINT('Ctrl Pts',(-20.7470624248403,21.9602064824542,-38.4199457671533));
#23300=CARTESIAN_POINT('Ctrl Pts',(-20.7480057020834,21.9585446690951,-38.4200645575819));
#23301=CARTESIAN_POINT('Ctrl Pts',(-20.7499210982433,21.9551772107352,-38.4203051958952));
#23302=CARTESIAN_POINT('Ctrl Pts',(-20.7508932981427,21.953471614259,-38.4204270383075));
#23303=CARTESIAN_POINT('Ctrl Pts',(-20.7533066120163,21.9492467514526,-38.4207287541832));
#23304=CARTESIAN_POINT('Ctrl Pts',(-20.7547495754288,21.9467285351042,-38.4209085072216));
#23305=CARTESIAN_POINT('Ctrl Pts',(-20.7601162927693,21.9373919622969,-38.4215746639933));
#23306=CARTESIAN_POINT('Ctrl Pts',(-20.7640616479999,21.9305859577467,-38.4220596762919));
#23307=CARTESIAN_POINT('Ctrl Pts',(-20.865048068485,21.757838506748,-38.4343568082435));
#23308=CARTESIAN_POINT('Ctrl Pts',(-20.9767357585437,21.6008661500425,-38.4452296503135));
#23309=CARTESIAN_POINT('Ctrl Pts',(-21.2664802519023,21.2623123414656,-38.4701930482823));
#23310=CARTESIAN_POINT('Ctrl Pts',(-21.453287296292,21.0899657653491,-38.4841816101874));
#23311=CARTESIAN_POINT('Ctrl Pts',(-21.6668370944805,20.9351093184205,-38.4997867690571));
#23312=CARTESIAN_POINT('Ctrl Pts',(-21.6753643779828,20.9289890686908,-38.5004091605558));
#23313=CARTESIAN_POINT('Ctrl Pts',(-21.72723932311,20.8921397235655,-38.5041913350193));
#23314=CARTESIAN_POINT('Ctrl Pts',(-21.771309573592,20.8624463063867,-38.5073874554204));
#23315=CARTESIAN_POINT('Ctrl Pts',(-21.8234604792933,20.8291529015466,-38.5111579670032));
#23316=CARTESIAN_POINT('Ctrl Pts',(-21.8308482100331,20.8244787395931,-38.511691828201));
#23317=CARTESIAN_POINT('Ctrl Pts',(-21.8418894549863,20.8175557748403,-38.5124893348566));
#23318=CARTESIAN_POINT('Ctrl Pts',(-21.8455286319444,20.8152840872476,-38.5127521322715));
#23319=CARTESIAN_POINT('Ctrl Pts',(-21.8520284827236,20.8112446912064,-38.5132214073414));
#23320=CARTESIAN_POINT('Ctrl Pts',(-21.8548874131356,20.8094741777601,-38.5134277810098));
#23321=CARTESIAN_POINT('Ctrl Pts',(-21.8608579327841,20.8057895974676,-38.5138586965083));
#23322=CARTESIAN_POINT('Ctrl Pts',(-21.8639700143954,20.8038763411756,-38.5140832678213));
#23323=CARTESIAN_POINT('Ctrl Pts',(-21.8721251831407,20.7988817657189,-38.5146716542104));
#23324=CARTESIAN_POINT('Ctrl Pts',(-21.8771734878629,20.795809030336,-38.5150357841794));
#23325=CARTESIAN_POINT('Ctrl Pts',(-21.8882200107703,20.7891269518107,-38.5158323565103));
#23326=CARTESIAN_POINT('Ctrl Pts',(-21.8942215836132,20.7855232382096,-38.5162650032033));
#23327=CARTESIAN_POINT('Ctrl Pts',(-21.9118186765147,20.7750347165431,-38.5175332032106));
#23328=CARTESIAN_POINT('Ctrl Pts',(-21.9234456182678,20.7682031653377,-38.5183706936456));
#23329=CARTESIAN_POINT('Ctrl Pts',(-21.963392287403,20.7450680573231,-38.5212467302993));
#23330=CARTESIAN_POINT('Ctrl Pts',(-21.9919161873216,20.7291227790547,-38.523298118158));
#23331=CARTESIAN_POINT('Ctrl Pts',(-22.1189053503157,20.6606475147691,-38.5324236795815));
#23332=CARTESIAN_POINT('Ctrl Pts',(-22.2198084383479,20.612824103726,-38.5396594003099));
#23333=CARTESIAN_POINT('Ctrl Pts',(-22.6380989874006,20.440552052251,-38.5695577646503));
#23334=CARTESIAN_POINT('Ctrl Pts',(-22.9717726182782,20.3615851558951,-38.5934515420524));
#23335=CARTESIAN_POINT('Ctrl Pts',(-23.3144541107854,20.3361391478788,-38.6151715652336));
#23336=CARTESIAN_POINT('Ctrl Pts',(-23.3173060645698,20.3359311907415,-38.6153521174194));
#23337=CARTESIAN_POINT('Ctrl Pts',(-23.3325205941522,20.3348421418486,-38.6163141789226));
#23338=CARTESIAN_POINT('Ctrl Pts',(-23.3448881268445,20.3340285586392,-38.6170921890727));
#23339=CARTESIAN_POINT('Ctrl Pts',(-23.3608562733654,20.3330705975283,-38.6180912415476));
#23340=CARTESIAN_POINT('Ctrl Pts',(-23.3644526447544,20.3328608952116,-38.6183158922679));
#23341=CARTESIAN_POINT('Ctrl Pts',(-23.3699530967615,20.3325494204645,-38.6186589287064));
#23342=CARTESIAN_POINT('Ctrl Pts',(-23.3718569134409,20.3324433077522,-38.6187775589311));
#23343=CARTESIAN_POINT('Ctrl Pts',(-23.3754354823829,20.332247035324,-38.6190003536484));
#23344=CARTESIAN_POINT('Ctrl Pts',(-23.3771102041661,20.3321564936849,-38.6191045392542));
#23345=CARTESIAN_POINT('Ctrl Pts',(-23.3809662197221,20.3319510420467,-38.6193442422244));
#23346=CARTESIAN_POINT('Ctrl Pts',(-23.3831475561887,20.331837042526,-38.6194797073406));
#23347=CARTESIAN_POINT('Ctrl Pts',(-23.3892242340005,20.3315256618876,-38.6198567110566));
#23348=CARTESIAN_POINT('Ctrl Pts',(-23.3931198369066,20.3313331335601,-38.6200979756529));
#23349=CARTESIAN_POINT('Ctrl Pts',(-23.4149260377442,20.3302951087031,-38.6214461703602));
#23350=CARTESIAN_POINT('Ctrl Pts',(-23.432843561434,20.3295920040264,-38.6225451885319));
#23351=CARTESIAN_POINT('Ctrl Pts',(-23.4847049261458,20.3279902845939,-38.6257033198866));
#23352=CARTESIAN_POINT('Ctrl Pts',(-23.5186593060064,20.3274784859633,-38.627742602826));
#23353=CARTESIAN_POINT('Ctrl Pts',(-23.6489224329086,20.327574053701,-38.6354788098027));
#23354=CARTESIAN_POINT('Ctrl Pts',(-23.7451844692565,20.3319615494773,-38.6410133377783));
#23355=CARTESIAN_POINT('Ctrl Pts',(-23.8708419267743,20.3433488686657,-38.6481604673383));
#23356=CARTESIAN_POINT('Ctrl Pts',(-23.9005329352196,20.3464559796316,-38.6498434572126));
#23357=CARTESIAN_POINT('Ctrl Pts',(-23.9549486958095,20.3529160040897,-38.6529236396775));
#23358=CARTESIAN_POINT('Ctrl Pts',(-23.9796857356447,20.3561443627306,-38.6543222325836));
#23359=CARTESIAN_POINT('Ctrl Pts',(-24.0256459794075,20.3626860761626,-38.6569212921574));
#23360=CARTESIAN_POINT('Ctrl Pts',(-24.0468782863967,20.365925019757,-38.6581221973717));
#23361=CARTESIAN_POINT('Ctrl Pts',(-24.0866552913762,20.3724004341239,-38.6603746233747));
#23362=CARTESIAN_POINT('Ctrl Pts',(-24.1052070535752,20.3755876117693,-38.6614262183962));
#23363=CARTESIAN_POINT('Ctrl Pts',(-24.2930132355238,20.4095490974281,-38.6720906220807));
#23364=CARTESIAN_POINT('Ctrl Pts',(-24.4595648318882,20.4536646830282,-38.6817217188843));
#23365=CARTESIAN_POINT('Ctrl Pts',(-24.7133213184869,20.5431263193665,-38.6973954523031));
#23366=CARTESIAN_POINT('Ctrl Pts',(-24.8033411230658,20.5795113506491,-38.7031605223613));
#23367=CARTESIAN_POINT('Ctrl Pts',(-24.900038843731,20.6237732309721,-38.7096337815531));
#23368=CARTESIAN_POINT('Ctrl Pts',(-24.9084846825761,20.6276835235829,-38.7102015549486));
#23369=CARTESIAN_POINT('Ctrl Pts',(-24.9210024574019,20.633545040314,-38.7110466518537));
#23370=CARTESIAN_POINT('Ctrl Pts',(-24.9250874743176,20.6354683494081,-38.7113230080222));
#23371=CARTESIAN_POINT('Ctrl Pts',(-24.9320748997358,20.6387761284917,-38.7117966969004));
#23372=CARTESIAN_POINT('Ctrl Pts',(-24.9349793110448,20.6401563735472,-38.7119938826647));
#23373=CARTESIAN_POINT('Ctrl Pts',(-24.940801325696,20.6429338221945,-38.7123897361764));
#23374=CARTESIAN_POINT('Ctrl Pts',(-24.9437189002218,20.6443310759816,-38.7125884054716));
#23375=CARTESIAN_POINT('Ctrl Pts',(-24.9495844178916,20.6471509921107,-38.712988410093));
#23376=CARTESIAN_POINT('Ctrl Pts',(-24.9525323067969,20.6485737574201,-38.7131897488243));
#23377=CARTESIAN_POINT('Ctrl Pts',(-24.9619282086737,20.6531262455882,-38.7138324580012));
#23378=CARTESIAN_POINT('Ctrl Pts',(-24.968367917015,20.6562729728153,-38.7142744220959));
#23379=CARTESIAN_POINT('Ctrl Pts',(-25.0062857236675,20.6749582468026,-38.7168854950162));
#23380=CARTESIAN_POINT('Ctrl Pts',(-25.037517721745,20.6909882945055,-38.7190717920934));
#23381=CARTESIAN_POINT('Ctrl Pts',(-25.127583706784,20.7390902328692,-38.725483780976));
#23382=CARTESIAN_POINT('Ctrl Pts',(-25.1856841218339,20.7724891232371,-38.7297559170129));
#23383=CARTESIAN_POINT('Ctrl Pts',(-25.3018723350526,20.8441888503961,-38.7385842224833));
#23384=CARTESIAN_POINT('Ctrl Pts',(-25.3598457257626,20.8826086231841,-38.743142740589));
#23385=CARTESIAN_POINT('Ctrl Pts',(-25.6718270883493,21.1042145419277,-38.7685065363326));
#23386=CARTESIAN_POINT('Ctrl Pts',(-25.8993107503608,21.3217797425351,-38.7903415970462));
#23387=CARTESIAN_POINT('Ctrl Pts',(-26.0945902405359,21.572252729701,-38.8106777682662));
#23388=CARTESIAN_POINT('Ctrl Pts',(-26.0973347423982,21.5757880965304,-38.81096391692));
#23389=CARTESIAN_POINT('Ctrl Pts',(-26.1032759194925,21.5834743053425,-38.8115840773288));
#23390=CARTESIAN_POINT('Ctrl Pts',(-26.1064698635435,21.5876272583711,-38.8119179268595));
#23391=CARTESIAN_POINT('Ctrl Pts',(-26.1149622516928,21.5987254569065,-38.8128067763762));
#23392=CARTESIAN_POINT('Ctrl Pts',(-26.1202426527369,21.6056845454561,-38.8133606751812));
#23393=CARTESIAN_POINT('Ctrl Pts',(-26.1262792062198,21.6137077124307,-38.8139952307614));
#23394=CARTESIAN_POINT('Ctrl Pts',(-26.1270630211751,21.6147507966916,-38.8140776506099));
#23395=CARTESIAN_POINT('Ctrl Pts',(-26.1359709452535,21.6266202746976,-38.8150146328091));
#23396=CARTESIAN_POINT('Ctrl Pts',(-26.1440275744639,21.6374974984242,-38.8158648613245));
#23397=CARTESIAN_POINT('Ctrl Pts',(-26.1541884732738,21.6513979474395,-38.8169403930653));
#23398=CARTESIAN_POINT('Ctrl Pts',(-26.1563562623996,21.6543742483854,-38.8171700435305));
#23399=CARTESIAN_POINT('Ctrl Pts',(-26.1597862583037,21.6591005157023,-38.8175337023592));
#23400=CARTESIAN_POINT('Ctrl Pts',(-26.1610518083004,21.6608480341763,-38.8176679435231));
#23401=CARTESIAN_POINT('Ctrl Pts',(-26.1634085349553,21.6641091790254,-38.8179180462281));
#23402=CARTESIAN_POINT('Ctrl Pts',(-26.1645001449014,21.6656224722222,-38.8180339377072));
#23403=CARTESIAN_POINT('Ctrl Pts',(-26.1669409214777,21.6690123091645,-38.8182931696697));
#23404=CARTESIAN_POINT('Ctrl Pts',(-26.1682893810629,21.6708893524445,-38.8184364604693));
#23405=CARTESIAN_POINT('Ctrl Pts',(-26.172252968614,21.6764191738728,-38.8188578605596));
#23406=CARTESIAN_POINT('Ctrl Pts',(-26.1748624931291,21.6800759905597,-38.8191355811265));
#23407=CARTESIAN_POINT('Ctrl Pts',(-26.1946258169644,21.7078938539758,-38.8212411515043));
#23408=CARTESIAN_POINT('Ctrl Pts',(-26.211454036139,21.732286010094,-38.8230469090003));
#23409=CARTESIAN_POINT('Ctrl Pts',(-26.2675138870268,21.8159904945888,-38.8291198742974));
#23410=CARTESIAN_POINT('Ctrl Pts',(-26.3051203927875,21.8763712069852,-38.8332932196779));
#23411=CARTESIAN_POINT('Ctrl Pts',(-26.4851727929966,22.1879921757956,-38.8540616426538));
#23412=CARTESIAN_POINT('Ctrl Pts',(-26.5953876040318,22.4563216130441,-38.869605038021));
#23413=CARTESIAN_POINT('Ctrl Pts',(-26.6731340114945,22.7539595137322,-38.8873491113756));
#23414=CARTESIAN_POINT('Ctrl Pts',(-26.6777279599063,22.7721980760058,-38.8884377699653));
#23415=CARTESIAN_POINT('Ctrl Pts',(-26.6880924048193,22.8149218026988,-38.89099219322));
#23416=CARTESIAN_POINT('Ctrl Pts',(-26.6937363310034,22.8394361639169,-38.8924611382815));
#23417=CARTESIAN_POINT('Ctrl Pts',(-26.7012419324503,22.8738759769489,-38.8945308265083));
#23418=CARTESIAN_POINT('Ctrl Pts',(-26.7033449037185,22.883748264714,-38.8951247950048));
#23419=CARTESIAN_POINT('Ctrl Pts',(-26.7195435886887,22.9615848847503,-38.8998137319719));
#23420=CARTESIAN_POINT('Ctrl Pts',(-26.7314857770043,23.0299743964491,-38.9039694122927));
#23421=CARTESIAN_POINT('Ctrl Pts',(-26.7424026479158,23.1071186682467,-38.9087149389453));
#23422=CARTESIAN_POINT('Ctrl Pts',(-26.743561671773,23.115549507629,-38.9092343240731));
#23423=CARTESIAN_POINT('Ctrl Pts',(-26.7452580762712,23.1282623000011,-38.9100186819118));
#23424=CARTESIAN_POINT('Ctrl Pts',(-26.745820277752,23.1325409498791,-38.9102828688248));
#23425=CARTESIAN_POINT('Ctrl Pts',(-26.7467796422115,23.1399575177152,-38.9107411613539));
#23426=CARTESIAN_POINT('Ctrl Pts',(-26.7471807836753,23.1430949229658,-38.910935140868));
#23427=CARTESIAN_POINT('Ctrl Pts',(-26.7479783796296,23.1494069264842,-38.9113256219343));
#23428=CARTESIAN_POINT('Ctrl Pts',(-26.7483747268683,23.1525815340213,-38.9115221266142));
#23429=CARTESIAN_POINT('Ctrl Pts',(-26.7491719705486,23.159045468068,-38.9119224693054));
#23430=CARTESIAN_POINT('Ctrl Pts',(-26.7495725221486,23.1623348323563,-38.9121263179657));
#23431=CARTESIAN_POINT('Ctrl Pts',(-26.7504850836596,23.1699264252955,-38.9125970695511));
#23432=CARTESIAN_POINT('Ctrl Pts',(-26.7509934915757,23.1742290732365,-38.9128640860952));
#23433=CARTESIAN_POINT('Ctrl Pts',(-26.7522813691773,23.1853202392472,-38.9135529389263));
#23434=CARTESIAN_POINT('Ctrl Pts',(-26.7530479247396,23.1921102090388,-38.9139751827672));
#23435=CARTESIAN_POINT('Ctrl Pts',(-26.7666711062891,23.3163237018742,-38.9217094353355));
#23436=CARTESIAN_POINT('Ctrl Pts',(-26.7730820564623,23.4343474892183,-38.9292245611143));
#23437=CARTESIAN_POINT('Ctrl Pts',(-26.7730017872581,23.5524430253128,-38.936921602977));
#23438=CARTESIAN_POINT('Ctrl Pts',(-26.7730017900261,23.5524389491122,-38.936921337305));
#23439=CARTESIAN_POINT('Ctrl Pts',(-26.7727891409872,23.8658807131493,-38.9573503324916));
#23440=CARTESIAN_POINT('Ctrl Pts',(-26.7268561765285,24.1775704728378,-38.9791096181834));
#23441=CARTESIAN_POINT('Ctrl Pts',(-26.6160288655546,24.5463820947226,-39.0044493874676));
#23442=CARTESIAN_POINT('Ctrl Pts',(-26.5931064491004,24.6143486286855,-39.009090152085));
#23443=CARTESIAN_POINT('Ctrl Pts',(-26.5639619025229,24.6920937661945,-39.0143204808516));
#23444=CARTESIAN_POINT('Ctrl Pts',(-26.559934520511,24.7026673493275,-39.0150301143754));
#23445=CARTESIAN_POINT('Ctrl Pts',(-26.5546481129803,24.7163296619211,-39.0159446246109));
#23446=CARTESIAN_POINT('Ctrl Pts',(-26.5534399273114,24.7194377820012,-39.0161525092692));
#23447=CARTESIAN_POINT('Ctrl Pts',(-26.5514781975387,24.7244613298895,-39.0164882363002));
#23448=CARTESIAN_POINT('Ctrl Pts',(-26.5507276428001,24.7263779105439,-39.0166162590548));
#23449=CARTESIAN_POINT('Ctrl Pts',(-26.5492865537635,24.7300474488885,-39.0168612512661));
#23450=CARTESIAN_POINT('Ctrl Pts',(-26.5485963205605,24.7318005146165,-39.0169782381755));
#23451=CARTESIAN_POINT('Ctrl Pts',(-26.5470102381166,24.735818533241,-39.017246248575));
#23452=CARTESIAN_POINT('Ctrl Pts',(-26.5461133561898,24.7380830816349,-39.0173972091676));
#23453=CARTESIAN_POINT('Ctrl Pts',(-26.5432769482755,24.7452211156974,-39.0178727726439));
#23454=CARTESIAN_POINT('Ctrl Pts',(-26.5413280786034,24.7500909160648,-39.0181968113259));
#23455=CARTESIAN_POINT('Ctrl Pts',(-26.525202563625,24.7901016052808,-39.0208559667316));
#23456=CARTESIAN_POINT('Ctrl Pts',(-26.5104182975749,24.8249965703154,-39.0231549691498));
#23457=CARTESIAN_POINT('Ctrl Pts',(-26.4934706601035,24.8631116924203,-39.0256523947349));
#23458=CARTESIAN_POINT('Ctrl Pts',(-26.4919138992812,24.8665961517352,-39.0258805801986));
#23459=CARTESIAN_POINT('Ctrl Pts',(-26.4310819913155,25.0021078691367,-39.0347501266444));
#23460=CARTESIAN_POINT('Ctrl Pts',(-26.3629799280313,25.1300107468675,-39.0429536562685));
#23461=CARTESIAN_POINT('Ctrl Pts',(-26.1965200527715,25.3975189945531,-39.0606290746895));
#23462=CARTESIAN_POINT('Ctrl Pts',(-26.0952190336246,25.5347598284421,-39.0700494660762));
#23463=CARTESIAN_POINT('Ctrl Pts',(-25.9492366651927,25.7028628382718,-39.0827526571655));
#23464=CARTESIAN_POINT('Ctrl Pts',(-25.9139686199556,25.7415311348619,-39.0857630114142));
#23465=CARTESIAN_POINT('Ctrl Pts',(-25.8295374576346,25.8296914466893,-39.092862098233));
#23466=CARTESIAN_POINT('Ctrl Pts',(-25.7796796035239,25.8784783461387,-39.0969746071866));
#23467=CARTESIAN_POINT('Ctrl Pts',(-25.7016089436013,25.9500634947489,-39.1033270409454));
#23468=CARTESIAN_POINT('Ctrl Pts',(-25.6745277880891,25.9740680240629,-39.1055154604634));
#23469=CARTESIAN_POINT('Ctrl Pts',(-25.6415560549796,26.0023168571015,-39.1081643955096));
#23470=CARTESIAN_POINT('Ctrl Pts',(-25.6360473262915,26.0070044434521,-39.1086064539987));
#23471=CARTESIAN_POINT('Ctrl Pts',(-25.6280177702024,26.0137906244364,-39.109250080421));
#23472=CARTESIAN_POINT('Ctrl Pts',(-25.6255094185427,26.0159040022403,-39.1094510410873));
#23473=CARTESIAN_POINT('Ctrl Pts',(-25.6205260466589,26.020089683396,-39.1098500928349));
#23474=CARTESIAN_POINT('Ctrl Pts',(-25.6180511303116,26.0221621049034,-39.1100481787474));
#23475=CARTESIAN_POINT('Ctrl Pts',(-25.6131121708935,26.0262852351134,-39.1104432891441));
#23476=CARTESIAN_POINT('Ctrl Pts',(-25.6106481731128,26.0283359927861,-39.1106403113213));
#23477=CARTESIAN_POINT('Ctrl Pts',(-25.6047348379815,26.0332426786641,-39.1111129200721));
#23478=CARTESIAN_POINT('Ctrl Pts',(-25.601282606284,26.0360950950138,-39.111388649283));
#23479=CARTESIAN_POINT('Ctrl Pts',(-25.5907528557781,26.0447584644402,-39.1122291140262));
#23480=CARTESIAN_POINT('Ctrl Pts',(-25.5836565506183,26.0505464172475,-39.1127947809014));
#23481=CARTESIAN_POINT('Ctrl Pts',(-25.5057535982969,26.1135353245246,-39.1189967396267));
#23482=CARTESIAN_POINT('Ctrl Pts',(-25.4325850893556,26.1677369212249,-39.1247524097535));
#23483=CARTESIAN_POINT('Ctrl Pts',(-25.2498357968397,26.2914849517779,-39.138986452077));
#23484=CARTESIAN_POINT('Ctrl Pts',(-25.1381642111273,26.357647894685,-39.1475729565328));
#23485=CARTESIAN_POINT('Ctrl Pts',(-24.9393873411553,26.4597576695493,-39.1625837392987));
#23486=CARTESIAN_POINT('Ctrl Pts',(-24.8541237161061,26.4989530784927,-39.1689401571942));
#23487=CARTESIAN_POINT('Ctrl Pts',(-24.5982850129614,26.6032924428686,-39.187635652949));
#23488=CARTESIAN_POINT('Ctrl Pts',(-24.4237251158533,26.6577413547762,-39.1999287861783));
#23489=CARTESIAN_POINT('Ctrl Pts',(-24.2299462023557,26.7005520439217,-39.2124813394223));
#23490=CARTESIAN_POINT('Ctrl Pts',(-24.2143910110535,26.7038680136092,-39.2134813542311));
#23491=CARTESIAN_POINT('Ctrl Pts',(-24.1951351060878,26.7078240850156,-39.2147093436109));
#23492=CARTESIAN_POINT('Ctrl Pts',(-24.1914573414103,26.708572977982,-39.2149434353068));
#23493=CARTESIAN_POINT('Ctrl Pts',(-24.1856689499649,26.7097411245297,-39.215311157281));
#23494=CARTESIAN_POINT('Ctrl Pts',(-24.1835592120875,26.7101646889385,-39.2154450348809));
#23495=CARTESIAN_POINT('Ctrl Pts',(-24.1796187297119,26.7109517003872,-39.2156948062384));
#23496=CARTESIAN_POINT('Ctrl Pts',(-24.1777881058823,26.7113156676249,-39.2158107292045));
#23497=CARTESIAN_POINT('Ctrl Pts',(-24.1736823269789,26.7121282772582,-39.2160704723937));
#23498=CARTESIAN_POINT('Ctrl Pts',(-24.1714070082653,26.7125760534678,-39.2162142420374));
#23499=CARTESIAN_POINT('Ctrl Pts',(-24.1656313986041,26.7137062029615,-39.2165787475968));
#23500=CARTESIAN_POINT('Ctrl Pts',(-24.1621304443666,26.7143852249228,-39.2167992911714));
#23501=CARTESIAN_POINT('Ctrl Pts',(-24.1429533793866,26.7180716635112,-39.2180051700298));
#23502=CARTESIAN_POINT('Ctrl Pts',(-24.1272558567958,26.7209684657301,-39.2189842572234));
#23503=CARTESIAN_POINT('Ctrl Pts',(-23.8073921281599,26.7775415842178,-39.2387843016447));
#23504=CARTESIAN_POINT('Ctrl Pts',(-23.4970366042432,26.7873434470794,-39.2553438885612));
#23505=CARTESIAN_POINT('Ctrl Pts',(-23.0649052344691,26.7387316725795,-39.2799150309674));
#23506=CARTESIAN_POINT('Ctrl Pts',(-22.9407654334487,26.7173461815343,-39.2871362177386));
#23507=CARTESIAN_POINT('Ctrl Pts',(-22.7762798230726,26.6789802059643,-39.2971246565931));
#23508=CARTESIAN_POINT('Ctrl Pts',(-22.7345597127801,26.668363430544,-39.2996946121722));
#23509=CARTESIAN_POINT('Ctrl Pts',(-22.6771076645535,26.6525113323316,-39.3032899199832));
#23510=CARTESIAN_POINT('Ctrl Pts',(-22.6611835555385,26.6479852453151,-39.3042924719312));
#23511=CARTESIAN_POINT('Ctrl Pts',(-22.6374843367405,26.6410514603901,-39.3057938222366));
#23512=CARTESIAN_POINT('Ctrl Pts',(-22.6296821643339,26.6387366246081,-39.3062896000534));
#23513=CARTESIAN_POINT('Ctrl Pts',(-22.6154953640493,26.6344689923783,-39.3071938651611));
#23514=CARTESIAN_POINT('Ctrl Pts',(-22.60910785923,26.6325258555983,-39.3076020349696));
#23515=CARTESIAN_POINT('Ctrl Pts',(-22.5990628602071,26.6294359402407,-39.3082455638051));
#23516=CARTESIAN_POINT('Ctrl Pts',(-22.5954012700646,26.6283024537349,-39.3084804859153));
#23517=CARTESIAN_POINT('Ctrl Pts',(-22.588853234784,26.626262627164,-39.3089012168007));
#23518=CARTESIAN_POINT('Ctrl Pts',(-22.5859660226315,26.6253587483755,-39.3090869444046));
#23519=CARTESIAN_POINT('Ctrl Pts',(-22.5798475825342,26.6234338280926,-39.3094809884327));
#23520=CARTESIAN_POINT('Ctrl Pts',(-22.5766166856722,26.6224117536565,-39.3096893386938));
#23521=CARTESIAN_POINT('Ctrl Pts',(-22.5673956480093,26.6194787277068,-39.3102847539681));
#23522=CARTESIAN_POINT('Ctrl Pts',(-22.5614095039608,26.61755534715,-39.310672228431));
#23523=CARTESIAN_POINT('Ctrl Pts',(-22.5357663752409,26.6092332022219,-39.3123361397588));
#23524=CARTESIAN_POINT('Ctrl Pts',(-22.5161659239285,26.6026630152079,-39.3136182299218));
#23525=CARTESIAN_POINT('Ctrl Pts',(-22.4922984392233,26.5944062256511,-39.3151922875919));
#23526=CARTESIAN_POINT('Ctrl Pts',(-22.4879697002519,26.592898380274,-39.3154782862847));
#23527=CARTESIAN_POINT('Ctrl Pts',(-22.3434652145688,26.5422166439851,-39.3250430756226));
#23528=CARTESIAN_POINT('Ctrl Pts',(-22.2069428185356,26.4834501520747,-39.3346403576747));
#23529=CARTESIAN_POINT('Ctrl Pts',(-22.0750358008163,26.4155366641038,-39.3444748119239));
#23530=CARTESIAN_POINT('Ctrl Pts',(-22.0750360153868,26.4155367745772,-39.5898217886697));
#23531=CARTESIAN_POINT('Ctrl Pts',(-22.0932423762876,26.4249104778562,-39.5885788452598));
#23532=CARTESIAN_POINT('Ctrl Pts',(-22.1115385781612,26.4341109096722,-39.5873456507141));
#23533=CARTESIAN_POINT('Ctrl Pts',(-22.1727952271205,26.4641863197141,-39.5832654164282));
#23534=CARTESIAN_POINT('Ctrl Pts',(-22.2161331629954,26.4842812843866,-39.5804575944052));
#23535=CARTESIAN_POINT('Ctrl Pts',(-22.3103876959713,26.5254647822196,-39.5744857489971));
#23536=CARTESIAN_POINT('Ctrl Pts',(-22.3614308422891,26.5462258643955,-39.5713341283085));
#23537=CARTESIAN_POINT('Ctrl Pts',(-22.512876291122,26.6033437788414,-39.5621557844431));
#23538=CARTESIAN_POINT('Ctrl Pts',(-22.6145825408525,26.6360325766563,-39.5562085348476));
#23539=CARTESIAN_POINT('Ctrl Pts',(-22.8619347815826,26.7021756726782,-39.5418976600202));
#23540=CARTESIAN_POINT('Ctrl Pts',(-23.008641590572,26.730669814653,-39.533526120418));
#23541=CARTESIAN_POINT('Ctrl Pts',(-23.2331159947678,26.7582825133143,-39.5204270958889));
#23542=CARTESIAN_POINT('Ctrl Pts',(-23.3097524252681,26.7649360772788,-39.5159068653008));
#23543=CARTESIAN_POINT('Ctrl Pts',(-23.4252767611635,26.7708118473049,-39.5089798669498));
#23544=CARTESIAN_POINT('Ctrl Pts',(-23.4640351215891,26.7720823854119,-39.5066369571666));
#23545=CARTESIAN_POINT('Ctrl Pts',(-23.5103790111826,26.7727647554029,-39.5038100036337));
#23546=CARTESIAN_POINT('Ctrl Pts',(-23.5179526148532,26.7728495656743,-39.5033472059705));
#23547=CARTESIAN_POINT('Ctrl Pts',(-23.5296072448996,26.7729389869574,-39.5026337581692));
#23548=CARTESIAN_POINT('Ctrl Pts',(-23.5336881341118,26.7729625461531,-39.5023837031664));
#23549=CARTESIAN_POINT('Ctrl Pts',(-23.5411134306535,26.7729913086406,-39.501928280077));
#23550=CARTESIAN_POINT('Ctrl Pts',(-23.5444578271249,26.7729990573871,-39.5017229922026));
#23551=CARTESIAN_POINT('Ctrl Pts',(-23.5511676688409,26.7730041589964,-39.5013107956578));
#23552=CARTESIAN_POINT('Ctrl Pts',(-23.5545331098365,26.7730014460947,-39.5011038851784));
#23553=CARTESIAN_POINT('Ctrl Pts',(-23.5640700551311,26.7729788195566,-39.5005170712636));
#23554=CARTESIAN_POINT('Ctrl Pts',(-23.5702414904978,26.772946450004,-39.5001367771977));
#23555=CARTESIAN_POINT('Ctrl Pts',(-23.5961264173647,26.7727363257548,-39.4985393192452));
#23556=CARTESIAN_POINT('Ctrl Pts',(-23.6158378276935,26.7723954145451,-39.497317044365));
#23557=CARTESIAN_POINT('Ctrl Pts',(-23.641491330684,26.771716241464,-39.4957184982719));
#23558=CARTESIAN_POINT('Ctrl Pts',(-23.647437658205,26.7715423358291,-39.4953474187107));
#23559=CARTESIAN_POINT('Ctrl Pts',(-23.661674775309,26.7710865017822,-39.4944576353208));
#23560=CARTESIAN_POINT('Ctrl Pts',(-23.6699649932557,26.7707890248447,-39.4939384469682));
#23561=CARTESIAN_POINT('Ctrl Pts',(-23.6829113594129,26.7702744142369,-39.4931259702669));
#23562=CARTESIAN_POINT('Ctrl Pts',(-23.6875683836914,26.7700791799857,-39.4928333672754));
#23563=CARTESIAN_POINT('Ctrl Pts',(-23.6956196694502,26.7697241505006,-39.4923269077802));
#23564=CARTESIAN_POINT('Ctrl Pts',(-23.6990141411132,26.7695690884279,-39.4921131988973));
#23565=CARTESIAN_POINT('Ctrl Pts',(-23.7037934309529,26.7693431917235,-39.4918120469891));
#23566=CARTESIAN_POINT('Ctrl Pts',(-23.705178467019,26.7692768310413,-39.4917247428162));
#23567=CARTESIAN_POINT('Ctrl Pts',(-23.9995241773085,26.7549835521879,-39.4731645087463));
#23568=CARTESIAN_POINT('Ctrl Pts',(-24.2891177986754,26.700831920194,-39.4533464569585));
#23569=CARTESIAN_POINT('Ctrl Pts',(-24.7321004770689,26.553502542047,-39.4217922953102));
#23570=CARTESIAN_POINT('Ctrl Pts',(-24.8922091912962,26.4854601227076,-39.410152826775));
#23571=CARTESIAN_POINT('Ctrl Pts',(-25.0553817782095,26.3999567288016,-39.3985564710867));
#23572=CARTESIAN_POINT('Ctrl Pts',(-25.0646689085598,26.3950321548831,-39.3978974588925));
#23573=CARTESIAN_POINT('Ctrl Pts',(-25.0767855816174,26.3885310412153,-39.3970391480163));
#23574=CARTESIAN_POINT('Ctrl Pts',(-25.0796369392056,26.3869956262303,-39.3968372739275));
#23575=CARTESIAN_POINT('Ctrl Pts',(-25.084291130095,26.3844803544605,-39.3965079432199));
#23576=CARTESIAN_POINT('Ctrl Pts',(-25.0860953416799,26.3835030740568,-39.3963803220784));
#23577=CARTESIAN_POINT('Ctrl Pts',(-25.0895563054749,26.3816241096321,-39.3961355984569));
#23578=CARTESIAN_POINT('Ctrl Pts',(-25.091213194494,26.3807226968873,-39.3960184794185));
#23579=CARTESIAN_POINT('Ctrl Pts',(-25.0950199253506,26.3786473524187,-39.3957494845215));
#23580=CARTESIAN_POINT('Ctrl Pts',(-25.0971692260515,26.3774724211297,-39.395597673103));
#23581=CARTESIAN_POINT('Ctrl Pts',(-25.1039803009785,26.3737390040052,-39.3951167849742));
#23582=CARTESIAN_POINT('Ctrl Pts',(-25.1086371142829,26.3711714128528,-39.3947882906196));
#23583=CARTESIAN_POINT('Ctrl Pts',(-25.1480604752523,26.3493074430281,-39.3920096607518));
#23584=CARTESIAN_POINT('Ctrl Pts',(-25.1824754282531,26.3293796231635,-39.3895993330433));
#23585=CARTESIAN_POINT('Ctrl Pts',(-25.2228016290224,26.305021310973,-39.3867826003589));
#23586=CARTESIAN_POINT('Ctrl Pts',(-25.2290756856143,26.3012022458936,-39.3863445871515));
#23587=CARTESIAN_POINT('Ctrl Pts',(-25.2364305515811,26.2966907513715,-39.3858313131038));
#23588=CARTESIAN_POINT('Ctrl Pts',(-25.2375240170949,26.2960191175163,-39.3857550084788));
#23589=CARTESIAN_POINT('Ctrl Pts',(-25.333492935482,26.236993633428,-39.3790584865481));
#23590=CARTESIAN_POINT('Ctrl Pts',(-25.4252886273435,26.1737555604773,-39.3726876067116));
#23591=CARTESIAN_POINT('Ctrl Pts',(-25.5746244884009,26.0590274272147,-39.3620627561516));
#23592=CARTESIAN_POINT('Ctrl Pts',(-25.6339209491184,26.0100004073171,-39.357767846591));
#23593=CARTESIAN_POINT('Ctrl Pts',(-25.8242447276136,25.8408129330366,-39.3435391570483));
#23594=CARTESIAN_POINT('Ctrl Pts',(-25.9470789984944,25.711947146339,-39.3335997846822));
#23595=CARTESIAN_POINT('Ctrl Pts',(-26.0933666167257,25.5305920858653,-39.3200190247008));
#23596=CARTESIAN_POINT('Ctrl Pts',(-26.126962173982,25.4866773058263,-39.3167604256944));
#23597=CARTESIAN_POINT('Ctrl Pts',(-26.1855328362358,25.4058914676214,-39.3108010774403));
#23598=CARTESIAN_POINT('Ctrl Pts',(-26.2109051593026,25.3693252179693,-39.3081161342583));
#23599=CARTESIAN_POINT('Ctrl Pts',(-26.2397644743913,25.3258375729456,-39.3049329174268));
#23600=CARTESIAN_POINT('Ctrl Pts',(-26.2439946899147,25.3194133248484,-39.3044629268465));
#23601=CARTESIAN_POINT('Ctrl Pts',(-26.2504297221017,25.3095641282728,-39.3037427324284));
#23602=CARTESIAN_POINT('Ctrl Pts',(-26.2526511322236,25.3061500107823,-39.3034931509501));
#23603=CARTESIAN_POINT('Ctrl Pts',(-26.2566844740497,25.2999253257613,-39.3030382253907));
#23604=CARTESIAN_POINT('Ctrl Pts',(-26.2584985177404,25.2971161279234,-39.3028329606348));
#23605=CARTESIAN_POINT('Ctrl Pts',(-26.2621319694266,25.2914701617539,-39.3024205003739));
#23606=CARTESIAN_POINT('Ctrl Pts',(-26.2639513064707,25.2886333529373,-39.3022133025649));
#23607=CARTESIAN_POINT('Ctrl Pts',(-26.2691021359829,25.2805741100404,-39.3016247798802));
#23608=CARTESIAN_POINT('Ctrl Pts',(-26.2724230120537,25.2753449379825,-39.3012430606711));
#23609=CARTESIAN_POINT('Ctrl Pts',(-26.2863492143308,25.2532758905025,-39.2996326182813));
#23610=CARTESIAN_POINT('Ctrl Pts',(-26.2968133345332,25.2363478270673,-39.2983986804764));
#23611=CARTESIAN_POINT('Ctrl Pts',(-26.4823487884561,24.9298920755265,-39.276080840194));
#23612=CARTESIAN_POINT('Ctrl Pts',(-26.6108687141934,24.6147254472101,-39.2531208396004));
#23613=CARTESIAN_POINT('Ctrl Pts',(-26.7062238952158,24.2077720078999,-39.2249467055564));
#23614=CARTESIAN_POINT('Ctrl Pts',(-26.7215394973034,24.1294134797271,-39.2196027893835));
#23615=CARTESIAN_POINT('Ctrl Pts',(-26.7450395194514,23.9798734724943,-39.2096430367205));
#23616=CARTESIAN_POINT('Ctrl Pts',(-26.7537919121531,23.9088265248681,-39.2050118618062));
#23617=CARTESIAN_POINT('Ctrl Pts',(-26.7611793656268,23.8262853865113,-39.1997915080681));
#23618=CARTESIAN_POINT('Ctrl Pts',(-26.7621275677949,23.8150241905454,-39.1990827309674));
#23619=CARTESIAN_POINT('Ctrl Pts',(-26.7632787348086,23.8004350483455,-39.1981691535799));
#23620=CARTESIAN_POINT('Ctrl Pts',(-26.7635357838307,23.7971116318246,-39.1979613529638));
#23621=CARTESIAN_POINT('Ctrl Pts',(-26.7639432008042,23.7917356189463,-39.1976257239533));
#23622=CARTESIAN_POINT('Ctrl Pts',(-26.7640967587815,23.7896832778982,-39.1974977153865));
#23623=CARTESIAN_POINT('Ctrl Pts',(-26.7643871408432,23.7857516341098,-39.1972527242374));
#23624=CARTESIAN_POINT('Ctrl Pts',(-26.7645242823066,23.7838723643227,-39.1971357242475));
#23625=CARTESIAN_POINT('Ctrl Pts',(-26.7648349807767,23.7795627521495,-39.1968676483867));
#23626=CARTESIAN_POINT('Ctrl Pts',(-26.7650074302428,23.7771323269742,-39.1967166355008));
#23627=CARTESIAN_POINT('Ctrl Pts',(-26.7655427103242,23.7694651784681,-39.1962407709202));
#23628=CARTESIAN_POINT('Ctrl Pts',(-26.7658955052301,23.7642277287888,-39.19591648442));
#23629=CARTESIAN_POINT('Ctrl Pts',(-26.7686960197496,23.7210805491599,-39.193251180697));
#23630=CARTESIAN_POINT('Ctrl Pts',(-26.7704861910868,23.6831291144767,-39.1909464627932));
#23631=CARTESIAN_POINT('Ctrl Pts',(-26.7717150203731,23.6414170278344,-39.1884481962684));
#23632=CARTESIAN_POINT('Ctrl Pts',(-26.7718185798421,23.6376809538629,-39.188224737885));
#23633=CARTESIAN_POINT('Ctrl Pts',(-26.7719484703991,23.6326809201674,-39.187926081204));
#23634=CARTESIAN_POINT('Ctrl Pts',(-26.7719805569873,23.6314171283385,-39.1878506279693));
#23635=CARTESIAN_POINT('Ctrl Pts',(-26.7722456878373,23.6207265223034,-39.1872126447667));
#23636=CARTESIAN_POINT('Ctrl Pts',(-26.7724381032979,23.6112986429933,-39.1866519056317));
#23637=CARTESIAN_POINT('Ctrl Pts',(-26.7726452285354,23.5983683715461,-39.185885281006));
#23638=CARTESIAN_POINT('Ctrl Pts',(-26.7726956116885,23.5948666896791,-39.1856779132015));
#23639=CARTESIAN_POINT('Ctrl Pts',(-26.7727895913231,23.5875003399322,-39.1852421819196));
#23640=CARTESIAN_POINT('Ctrl Pts',(-26.7728319437466,23.5836356589857,-39.1850138694899));
#23641=CARTESIAN_POINT('Ctrl Pts',(-26.7729526730352,23.570455253057,-39.1842361747661));
#23642=CARTESIAN_POINT('Ctrl Pts',(-26.7729976092543,23.5611391940742,-39.1836881261123));
#23643=CARTESIAN_POINT('Ctrl Pts',(-26.7730486752823,23.4563455716258,-39.1775403865788));
#23644=CARTESIAN_POINT('Ctrl Pts',(-26.7688522351414,23.3609065026718,-39.1721002447795));
#23645=CARTESIAN_POINT('Ctrl Pts',(-26.7402590594943,23.0382326593435,-39.1538455788826));
#23646=CARTESIAN_POINT('Ctrl Pts',(-26.6959581266797,22.813475199057,-39.1413157819931));
#23647=CARTESIAN_POINT('Ctrl Pts',(-26.5937217524624,22.4839492165254,-39.1213777090175));
#23648=CARTESIAN_POINT('Ctrl Pts',(-26.5531658202046,22.3745762778425,-39.1144919655493));
#23649=CARTESIAN_POINT('Ctrl Pts',(-26.5025603998996,22.2579258944259,-39.1067546974105));
#23650=CARTESIAN_POINT('Ctrl Pts',(-26.4982945552024,22.2482240721448,-39.1061081773821));
#23651=CARTESIAN_POINT('Ctrl Pts',(-26.4922346207983,22.2346244081838,-39.1051976104198));
#23652=CARTESIAN_POINT('Ctrl Pts',(-26.4904804511666,22.2307087646117,-39.1049349355158));
#23653=CARTESIAN_POINT('Ctrl Pts',(-26.4874221406496,22.2239184050482,-39.1044785370549));
#23654=CARTESIAN_POINT('Ctrl Pts',(-26.4861215826788,22.2210420733241,-39.1042849370573));
#23655=CARTESIAN_POINT('Ctrl Pts',(-26.4834060626907,22.2150598208892,-39.1038817112614));
#23656=CARTESIAN_POINT('Ctrl Pts',(-26.4819903893174,22.2119542295871,-39.1036720611305));
#23657=CARTESIAN_POINT('Ctrl Pts',(-26.4786440768848,22.2046441467181,-39.1031778154211));
#23658=CARTESIAN_POINT('Ctrl Pts',(-26.4767093157951,22.2004415604487,-39.1028930776483));
#23659=CARTESIAN_POINT('Ctrl Pts',(-26.47034901248,22.1867039968745,-39.1019603595255));
#23660=CARTESIAN_POINT('Ctrl Pts',(-26.465885901955,22.1771865791904,-39.101311078936));
#23661=CARTESIAN_POINT('Ctrl Pts',(-26.4031269685584,22.0450412420135,-39.0922525295016));
#23662=CARTESIAN_POINT('Ctrl Pts',(-26.3371929966061,21.9262120128547,-39.083574323288));
#23663=CARTESIAN_POINT('Ctrl Pts',(-26.1603722218138,21.6501784685629,-39.0620637524151));
#23664=CARTESIAN_POINT('Ctrl Pts',(-26.042530731541,21.4980482048361,-39.049027721206));
#23665=CARTESIAN_POINT('Ctrl Pts',(-25.8083654898574,21.2458700797627,-39.0257643943012));
#23666=CARTESIAN_POINT('Ctrl Pts',(-25.69709503596,21.1418651779893,-39.0155550452248));
#23667=CARTESIAN_POINT('Ctrl Pts',(-25.5757858851582,21.0435917876213,-39.0055631286601));
#23668=CARTESIAN_POINT('Ctrl Pts',(-25.5726838864335,21.0410883546052,-39.0053083481025));
#23669=CARTESIAN_POINT('Ctrl Pts',(-25.5656343491558,21.035420670997,-39.0047309924384));
#23670=CARTESIAN_POINT('Ctrl Pts',(-25.5616839760502,21.0322599377526,-39.0044086295388));
#23671=CARTESIAN_POINT('Ctrl Pts',(-25.550677867339,21.0234962683389,-39.0035137874245));
#23672=CARTESIAN_POINT('Ctrl Pts',(-25.5436059895911,21.0179135468737,-39.0029425607112));
#23673=CARTESIAN_POINT('Ctrl Pts',(-25.5251747178205,21.0034884793743,-39.0014636893473));
#23674=CARTESIAN_POINT('Ctrl Pts',(-25.5137791653583,20.9946923275849,-39.0005590428813));
#23675=CARTESIAN_POINT('Ctrl Pts',(-25.499326542693,20.9836901885431,-38.9994242929052));
#23676=CARTESIAN_POINT('Ctrl Pts',(-25.4963242607295,20.9814129906899,-38.9991892481636));
#23677=CARTESIAN_POINT('Ctrl Pts',(-25.4915805624859,20.977828036794,-38.9988189509027));
#23678=CARTESIAN_POINT('Ctrl Pts',(-25.4898418148762,20.9765167803526,-38.9986834511783));
#23679=CARTESIAN_POINT('Ctrl Pts',(-25.4866118939054,20.9740861047065,-38.9984321708902));
#23680=CARTESIAN_POINT('Ctrl Pts',(-25.4851210872734,20.9729662240006,-38.9983163578943));
#23681=CARTESIAN_POINT('Ctrl Pts',(-25.4818003558064,20.970476225221,-38.9980587612886));
#23682=CARTESIAN_POINT('Ctrl Pts',(-25.4799699490454,20.9691067633343,-38.9979170244393));
#23683=CARTESIAN_POINT('Ctrl Pts',(-25.4746347209277,20.9651239341897,-38.9975046212025));
#23684=CARTESIAN_POINT('Ctrl Pts',(-25.4711260192739,20.962515736515,-38.9972343187156));
#23685=CARTESIAN_POINT('Ctrl Pts',(-25.4462009303649,20.9440662686637,-38.9953205314022));
#23686=CARTESIAN_POINT('Ctrl Pts',(-25.4245933479867,20.928483322992,-38.9936948383992));
#23687=CARTESIAN_POINT('Ctrl Pts',(-25.3742452377572,20.8931139508161,-38.9899768912755));
#23688=CARTESIAN_POINT('Ctrl Pts',(-25.345371257397,20.8735224746188,-38.9878962927704));
#23689=CARTESIAN_POINT('Ctrl Pts',(-25.2507200066345,20.8115206530372,-38.9812216896764));
#23690=CARTESIAN_POINT('Ctrl Pts',(-25.1837117962571,20.7710342353063,-38.97671980131));
#23691=CARTESIAN_POINT('Ctrl Pts',(-24.8016863189287,20.5588096233239,-38.951903108673));
#23692=CARTESIAN_POINT('Ctrl Pts',(-24.4612266344838,20.4381874504242,-38.9325812485604));
#23693=CARTESIAN_POINT('Ctrl Pts',(-24.087748730154,20.3725751907067,-38.9096500643141));
#23694=CARTESIAN_POINT('Ctrl Pts',(-24.067582021627,20.369229800607,-38.9084079163962));
#23695=CARTESIAN_POINT('Ctrl Pts',(-24.0411998473406,20.3651108571395,-38.9067773781893));
#23696=CARTESIAN_POINT('Ctrl Pts',(-24.0350117230723,20.3641631922019,-38.9063945261255));
#23697=CARTESIAN_POINT('Ctrl Pts',(-24.0254750845162,20.3627311537633,-38.9058038798318));
#23698=CARTESIAN_POINT('Ctrl Pts',(-24.0221284789622,20.3622340092059,-38.9055964911678));
#23699=CARTESIAN_POINT('Ctrl Pts',(-24.0154736029002,20.36125612323,-38.905183851314));
#23700=CARTESIAN_POINT('Ctrl Pts',(-24.0121653546962,20.3607752575779,-38.9049786043428));
#23701=CARTESIAN_POINT('Ctrl Pts',(-24.0049265917876,20.3597345762591,-38.9045292460742));
#23702=CARTESIAN_POINT('Ctrl Pts',(-24.0009957828965,20.3591768750941,-38.9042850680633));
#23703=CARTESIAN_POINT('Ctrl Pts',(-23.9898145414582,20.3576115581056,-38.9035900214863));
#23704=CARTESIAN_POINT('Ctrl Pts',(-23.9825617271207,20.3566213844266,-38.9031386009302));
#23705=CARTESIAN_POINT('Ctrl Pts',(-23.9662991876153,20.3544575922485,-38.9021251012972));
#23706=CARTESIAN_POINT('Ctrl Pts',(-23.9572877731582,20.3532973514679,-38.9015626017115));
#23707=CARTESIAN_POINT('Ctrl Pts',(-23.7642331733247,20.3292705960213,-38.8894923430329));
#23708=CARTESIAN_POINT('Ctrl Pts',(-23.5785951476054,20.3222984865728,-38.8774724276307));
#23709=CARTESIAN_POINT('Ctrl Pts',(-23.135048398545,20.3439096130843,-38.8478493236458));
#23710=CARTESIAN_POINT('Ctrl Pts',(-22.8791498539228,20.3875564603773,-38.8299819763953));
#23711=CARTESIAN_POINT('Ctrl Pts',(-22.6268057410478,20.4626345424977,-38.8128087988759));
#23712=CARTESIAN_POINT('Ctrl Pts',(-22.6223891570548,20.4639589000362,-38.8125084032396));
#23713=CARTESIAN_POINT('Ctrl Pts',(-22.6152632715626,20.4661123478861,-38.812024029301));
#23714=CARTESIAN_POINT('Ctrl Pts',(-22.6125522086587,20.4669355362774,-38.8118398171331));
#23715=CARTESIAN_POINT('Ctrl Pts',(-22.6065830618418,20.468756611695,-38.8114343813186));
#23716=CARTESIAN_POINT('Ctrl Pts',(-22.6033254635168,20.4697560942601,-38.8112132226204));
#23717=CARTESIAN_POINT('Ctrl Pts',(-22.551863483497,20.4856347867528,-38.8077211652514));
#23718=CARTESIAN_POINT('Ctrl Pts',(-22.5040099610582,20.5016397635422,-38.8044975096326));
#23719=CARTESIAN_POINT('Ctrl Pts',(-22.4517385317311,20.520498299976,-38.8010173840174));
#23720=CARTESIAN_POINT('Ctrl Pts',(-22.4469323844136,20.5222452057141,-38.8006977880717));
#23721=CARTESIAN_POINT('Ctrl Pts',(-22.4397866227068,20.5248617706211,-38.8002232130513));
#23722=CARTESIAN_POINT('Ctrl Pts',(-22.4374438571534,20.5257227093614,-38.8000677177786));
#23723=CARTESIAN_POINT('Ctrl Pts',(-22.4334274688164,20.5272039830913,-38.7998013075428));
#23724=CARTESIAN_POINT('Ctrl Pts',(-22.4317533616541,20.52782298662,-38.7996903126786));
#23725=CARTESIAN_POINT('Ctrl Pts',(-22.4284823478305,20.5290355385796,-38.799473540385));
#23726=CARTESIAN_POINT('Ctrl Pts',(-22.4268854016135,20.5296289609801,-38.7993677559942));
#23727=CARTESIAN_POINT('Ctrl Pts',(-22.4230151135705,20.5310706469291,-38.7991114925794));
#23728=CARTESIAN_POINT('Ctrl Pts',(-22.4207422523699,20.5319202141542,-38.7989610923702));
#23729=CARTESIAN_POINT('Ctrl Pts',(-22.4137314264188,20.5345498015775,-38.7984974506926));
#23730=CARTESIAN_POINT('Ctrl Pts',(-22.4089966644922,20.536338427813,-38.7981847252591));
#23731=CARTESIAN_POINT('Ctrl Pts',(-22.3557718815407,20.5565882831664,-38.7946735295146));
#23732=CARTESIAN_POINT('Ctrl Pts',(-22.3077268482433,20.5762080898295,-38.7915436464208));
#23733=CARTESIAN_POINT('Ctrl Pts',(-22.207509093983,20.6199862666761,-38.7850569635846));
#23734=CARTESIAN_POINT('Ctrl Pts',(-22.1554667641143,20.6443974588126,-38.7817131058483));
#23735=CARTESIAN_POINT('Ctrl Pts',(-21.7564467706001,20.8447550983272,-38.7560618987133));
#23736=CARTESIAN_POINT('Ctrl Pts',(-21.4432808432482,21.0808065500301,-38.7354008162317));
#23737=CARTESIAN_POINT('Ctrl Pts',(-21.166264554272,21.3815864747838,-38.7106641527116));
#23738=CARTESIAN_POINT('Ctrl Pts',(-21.1529599503505,21.3963028120065,-38.7094584087346));
#23739=CARTESIAN_POINT('Ctrl Pts',(-21.135685705938,21.4157683119338,-38.7078690852102));
#23740=CARTESIAN_POINT('Ctrl Pts',(-21.1315924744366,21.4204076155015,-38.7074907013341));
#23741=CARTESIAN_POINT('Ctrl Pts',(-21.1252913105234,21.4275909982777,-38.7069054356348));
#23742=CARTESIAN_POINT('Ctrl Pts',(-21.1230739495771,21.4301268184397,-38.7066989474958));
#23743=CARTESIAN_POINT('Ctrl Pts',(-21.1186632261384,21.4351870020044,-38.7062871357867));
#23744=CARTESIAN_POINT('Ctrl Pts',(-21.1164698088574,21.4377113122944,-38.706081814864));
#23745=CARTESIAN_POINT('Ctrl Pts',(-21.1116658369091,21.4432574104965,-38.7056309575757));
#23746=CARTESIAN_POINT('Ctrl Pts',(-21.1090569644764,21.4462806423617,-38.705385351923));
#23747=CARTESIAN_POINT('Ctrl Pts',(-21.1016265954841,21.4549235801813,-38.7046836578551));
#23748=CARTESIAN_POINT('Ctrl Pts',(-21.0968188619471,21.4605550375067,-38.7042270019769));
#23749=CARTESIAN_POINT('Ctrl Pts',(-21.0860627788269,21.4732422786722,-38.7031993862068));
#23750=CARTESIAN_POINT('Ctrl Pts',(-21.0801252614929,21.4803071228846,-38.7026279858899));
#23751=CARTESIAN_POINT('Ctrl Pts',(-20.9346536369767,21.6549159517201,-38.6885254399982));
#23752=CARTESIAN_POINT('Ctrl Pts',(-20.8124781729958,21.8361302177024,-38.674274671901));
#23753=CARTESIAN_POINT('Ctrl Pts',(-20.5888384101235,22.253538310913,-38.6424530666805));
#23754=CARTESIAN_POINT('Ctrl Pts',(-20.4953589859098,22.4923880830987,-38.6248339770699));
#23755=CARTESIAN_POINT('Ctrl Pts',(-20.4289638884117,22.7479150490506,-38.6079130829125));
#23756=CARTESIAN_POINT('Ctrl Pts',(-20.426881611823,22.7560596515223,-38.6073757882279));
#23757=CARTESIAN_POINT('Ctrl Pts',(-20.4187807501092,22.7882699738928,-38.6052591834939));
#23758=CARTESIAN_POINT('Ctrl Pts',(-20.4130080408678,22.8123975095682,-38.6036919675688));
#23759=CARTESIAN_POINT('Ctrl Pts',(-20.406595243375,22.8406373960494,-38.6018808046979));
#23760=CARTESIAN_POINT('Ctrl Pts',(-20.4056840016763,22.8446864131629,-38.6016216754846));
#23761=CARTESIAN_POINT('Ctrl Pts',(-20.4042428745779,22.8511481748732,-38.6012090314488));
#23762=CARTESIAN_POINT('Ctrl Pts',(-20.4037079409947,22.8535597706917,-38.6010552273767));
#23763=CARTESIAN_POINT('Ctrl Pts',(-20.4027687313411,22.857817076903,-38.6007840635495));
#23764=CARTESIAN_POINT('Ctrl Pts',(-20.4023633053635,22.8596625293318,-38.6006666371014));
#23765=CARTESIAN_POINT('Ctrl Pts',(-20.4015230093326,22.8635035754098,-38.6004224759807));
#23766=CARTESIAN_POINT('Ctrl Pts',(-20.4010884141573,22.865499222229,-38.6002957575149));
#23767=CARTESIAN_POINT('Ctrl Pts',(-20.3999643607833,22.8706845424272,-38.5999668567238));
#23768=CARTESIAN_POINT('Ctrl Pts',(-20.3992778474872,22.8738748623933,-38.5997648448158));
#23769=CARTESIAN_POINT('Ctrl Pts',(-20.3963676842562,22.8874993739185,-38.5989035991954));
#23770=CARTESIAN_POINT('Ctrl Pts',(-20.3941909739352,22.8979436859525,-38.5982470423296));
#23771=CARTESIAN_POINT('Ctrl Pts',(-20.360075847711,23.0658042439155,-38.5877507659688));
#23772=CARTESIAN_POINT('Ctrl Pts',(-20.3398931067016,23.2254060633344,-38.5785542679436));
#23773=CARTESIAN_POINT('Ctrl Pts',(-20.3160933883911,23.6913918255792,-38.552281188942));
#23774=CARTESIAN_POINT('Ctrl Pts',(-20.3440673797946,23.9975471959323,-38.5355747057476));
#23775=CARTESIAN_POINT('Ctrl Pts',(-20.415308618021,24.2974135211587,-38.5171371937451));
#23776=CARTESIAN_POINT('Ctrl Pts',(-20.4158443398733,24.2996577445527,-38.5169990967291));
#23777=CARTESIAN_POINT('Ctrl Pts',(-20.4174801052446,24.3064777857092,-38.5165790954939));
#23778=CARTESIAN_POINT('Ctrl Pts',(-20.4185877589123,24.3110517570495,-38.5162969577598));
#23779=CARTESIAN_POINT('Ctrl Pts',(-20.4224628120379,24.3269016397078,-38.5153176817106));
#23780=CARTESIAN_POINT('Ctrl Pts',(-20.4252811017223,24.3381649150901,-38.5146189711511));
#23781=CARTESIAN_POINT('Ctrl Pts',(-20.4293296674554,24.3539815162727,-38.5136337349374));
#23782=CARTESIAN_POINT('Ctrl Pts',(-20.4305091918925,24.3585478357641,-38.5133488157572));
#23783=CARTESIAN_POINT('Ctrl Pts',(-20.4367996007471,24.3826811460373,-38.5118404494558));
#23784=CARTESIAN_POINT('Ctrl Pts',(-20.442084469958,24.4022019563733,-38.5106114983937));
#23785=CARTESIAN_POINT('Ctrl Pts',(-20.4492382432972,24.4276730734682,-38.508995889728));
#23786=CARTESIAN_POINT('Ctrl Pts',(-20.4509412653042,24.4336698153914,-38.5086146448955));
#23787=CARTESIAN_POINT('Ctrl Pts',(-20.4535939263364,24.4429083754428,-38.5080259340157));
#23788=CARTESIAN_POINT('Ctrl Pts',(-20.4545312878063,24.4461537279864,-38.5078188692428));
#23789=CARTESIAN_POINT('Ctrl Pts',(-20.4564065506702,24.4526082190238,-38.5074065293576));
#23790=CARTESIAN_POINT('Ctrl Pts',(-20.4573443469707,24.4558173838672,-38.5072012579016));
#23791=CARTESIAN_POINT('Ctrl Pts',(-20.4594089869835,24.462842018948,-38.5067513684569));
#23792=CARTESIAN_POINT('Ctrl Pts',(-20.4605379041815,24.4666568695458,-38.5065066828386));
#23793=CARTESIAN_POINT('Ctrl Pts',(-20.4637719750084,24.4775115715444,-38.5058094130951));
#23794=CARTESIAN_POINT('Ctrl Pts',(-20.4658941350117,24.4845462934012,-38.5053562719896));
#23795=CARTESIAN_POINT('Ctrl Pts',(-20.47070837086,24.5003097732951,-38.5043380271204));
#23796=CARTESIAN_POINT('Ctrl Pts',(-20.4734135288772,24.5090344405901,-38.5037724958873));
#23797=CARTESIAN_POINT('Ctrl Pts',(-20.4819653883701,24.5362069294395,-38.5020049991495));
#23798=CARTESIAN_POINT('Ctrl Pts',(-20.4879411037314,24.5546134031521,-38.5007987964809));
#23799=CARTESIAN_POINT('Ctrl Pts',(-20.5109360472797,24.6233291898409,-38.4962617079172));
#23800=CARTESIAN_POINT('Ctrl Pts',(-20.5290315062651,24.6732668611825,-38.4928956075717));
#23801=CARTESIAN_POINT('Ctrl Pts',(-20.5686608925694,24.7747300028441,-38.4859109089954));
#23802=CARTESIAN_POINT('Ctrl Pts',(-20.5903166641487,24.826188605418,-38.4822893721913));
#23803=CARTESIAN_POINT('Ctrl Pts',(-20.7551474692525,25.1910508948088,-38.4560472467813));
#23804=CARTESIAN_POINT('Ctrl Pts',(-20.9464020619259,25.4802129667489,-38.4319036663617));
#23805=CARTESIAN_POINT('Ctrl Pts',(-21.2026393636181,25.7584120557744,-38.4076428558123));
#23806=CARTESIAN_POINT('Ctrl Pts',(-21.2258881765836,25.7828713168629,-38.4055023383247));
#23807=CARTESIAN_POINT('Ctrl Pts',(-21.2530684231166,25.810581809001,-38.4030732725928));
#23808=CARTESIAN_POINT('Ctrl Pts',(-21.2566274413075,25.8141931705223,-38.402756625475));
#23809=CARTESIAN_POINT('Ctrl Pts',(-21.2619034981501,25.819521612122,-38.4022893260839));
#23810=CARTESIAN_POINT('Ctrl Pts',(-21.2636139562817,25.8212451526063,-38.402138158058));
#23811=CARTESIAN_POINT('Ctrl Pts',(-21.2666504141445,25.8242979262086,-38.4018703817965));
#23812=CARTESIAN_POINT('Ctrl Pts',(-21.2679756270664,25.8256279333065,-38.4017537112319));
#23813=CARTESIAN_POINT('Ctrl Pts',(-21.2707736612757,25.8284311861039,-38.4015077888508));
#23814=CARTESIAN_POINT('Ctrl Pts',(-21.2722467452791,25.829904158415,-38.4013785589503));
#23815=CARTESIAN_POINT('Ctrl Pts',(-21.2761599208513,25.8338094567587,-38.4010359018618));
#23816=CARTESIAN_POINT('Ctrl Pts',(-21.2786024949575,25.8362393084623,-38.4008226726297));
#23817=CARTESIAN_POINT('Ctrl Pts',(-21.2898426114642,25.8473850743172,-38.3998444210227));
#23818=CARTESIAN_POINT('Ctrl Pts',(-21.2986866049169,25.8560543043904,-38.3990830648251));
#23819=CARTESIAN_POINT('Ctrl Pts',(-21.5200191545621,26.070525454943,-38.3802290907101));
#23820=CARTESIAN_POINT('Ctrl Pts',(-21.7598298502829,26.2461899450686,-38.3642695403191));
#23821=CARTESIAN_POINT('Ctrl Pts',(-22.0384463579977,26.3964755451759,-38.3464523789056));
#23822=CARTESIAN_POINT('Ctrl Pts',(-22.0566974805562,26.4060950207338,-38.3452888360464));
#23823=CARTESIAN_POINT('Ctrl Pts',(-22.0750360565132,26.4155367957515,-38.344122456765));
#23824=CARTESIAN_POINT('Origin',(-23.5502525316942,23.5502525316942,-77.3107734492734));
#23825=CARTESIAN_POINT('',(-22.0750359454076,26.4155367385478,-36.8487079434683));
#23826=CARTESIAN_POINT('',(-22.0750364532454,26.4155370000125,-37.0955933117774));
#23827=CARTESIAN_POINT('',(-22.0750360153461,26.4155367745563,-77.3107734492734));
#23828=CARTESIAN_POINT('Ctrl Pts',(-22.0750359454076,26.4155367385478,-36.8487079434683));
#23829=CARTESIAN_POINT('Ctrl Pts',(-21.9862064593613,26.3698021022233,-36.8544705918441));
#23830=CARTESIAN_POINT('Ctrl Pts',(-21.8995139251075,26.3199418552687,-36.8600951447363));
#23831=CARTESIAN_POINT('Ctrl Pts',(-21.6884902932866,26.1851307091665,-36.8741149760281));
#23832=CARTESIAN_POINT('Ctrl Pts',(-21.5675611975838,26.0953802592486,-36.8824619548554));
#23833=CARTESIAN_POINT('Ctrl Pts',(-21.3786124843708,25.9334819647741,-36.8966333656106));
#23834=CARTESIAN_POINT('Ctrl Pts',(-21.3068569595978,25.8660627417802,-36.9023222916117));
#23835=CARTESIAN_POINT('Ctrl Pts',(-21.1938838215147,25.7497318017075,-36.9119171374906));
#23836=CARTESIAN_POINT('Ctrl Pts',(-21.1508352023558,25.7026879366804,-36.9157428737853));
#23837=CARTESIAN_POINT('Ctrl Pts',(-21.1037257343339,25.6480358391879,-36.9201410790945));
#23838=CARTESIAN_POINT('Ctrl Pts',(-21.0982642369984,25.6416495709885,-36.9206543240258));
#23839=CARTESIAN_POINT('Ctrl Pts',(-21.0900967532386,25.6320231550633,-36.9214269542763));
#23840=CARTESIAN_POINT('Ctrl Pts',(-21.0873720246064,25.6287988963756,-36.9216855679607));
#23841=CARTESIAN_POINT('Ctrl Pts',(-21.0826963264578,25.6232438908574,-36.9221308401683));
#23842=CARTESIAN_POINT('Ctrl Pts',(-21.0807423000963,25.6209157146127,-36.9223173730561));
#23843=CARTESIAN_POINT('Ctrl Pts',(-21.0767244653231,25.6161147829647,-36.9227018462092));
#23844=CARTESIAN_POINT('Ctrl Pts',(-21.07466106479,25.6136416915994,-36.9228998028758));
#23845=CARTESIAN_POINT('Ctrl Pts',(-21.0697018152412,25.6076796299177,-36.9233768031177));
#23846=CARTESIAN_POINT('Ctrl Pts',(-21.066809620837,25.6041876401109,-36.9236559952858));
#23847=CARTESIAN_POINT('Ctrl Pts',(-21.0579538920438,25.5934493226209,-36.9245139804155));
#23848=CARTESIAN_POINT('Ctrl Pts',(-21.0520146728033,25.5861830887293,-36.925093758863));
#23849=CARTESIAN_POINT('Ctrl Pts',(-21.0302201504765,25.5592799971502,-36.9272375597684));
#23850=CARTESIAN_POINT('Ctrl Pts',(-21.0145642756995,25.5394834306282,-36.9288095747776));
#23851=CARTESIAN_POINT('Ctrl Pts',(-20.9954523337661,25.5147244681888,-36.9307693378903));
#23852=CARTESIAN_POINT('Ctrl Pts',(-20.9917752519811,25.509933130414,-36.9311483004828));
#23853=CARTESIAN_POINT('Ctrl Pts',(-20.9839470684788,25.4996732069322,-36.9319591822748));
#23854=CARTESIAN_POINT('Ctrl Pts',(-20.9797999353628,25.4942016432743,-36.9323912537161));
#23855=CARTESIAN_POINT('Ctrl Pts',(-20.9747802443278,25.4875347128332,-36.9329172794883));
#23856=CARTESIAN_POINT('Ctrl Pts',(-20.973890960488,25.4863519110524,-36.9330105866549));
#23857=CARTESIAN_POINT('Ctrl Pts',(-20.9691736348736,25.4800685748094,-36.9335061686704));
#23858=CARTESIAN_POINT('Ctrl Pts',(-20.9653599454045,25.4749573267952,-36.9339089948932));
#23859=CARTESIAN_POINT('Ctrl Pts',(-20.9559620080961,25.4622835506337,-36.9349070787097));
#23860=CARTESIAN_POINT('Ctrl Pts',(-20.9503956579061,25.4547078793064,-36.9355030127565));
#23861=CARTESIAN_POINT('Ctrl Pts',(-20.9425193889019,25.4438895791304,-36.936353094461));
#23862=CARTESIAN_POINT('Ctrl Pts',(-20.9401821716337,25.440666805537,-36.9366062169893));
#23863=CARTESIAN_POINT('Ctrl Pts',(-20.934802916789,25.4332203932271,-36.9371908034007));
#23864=CARTESIAN_POINT('Ctrl Pts',(-20.9317651341023,25.4289937070079,-36.9375224241165));
#23865=CARTESIAN_POINT('Ctrl Pts',(-20.9149059765851,25.4054160255719,-36.939371201553));
#23866=CARTESIAN_POINT('Ctrl Pts',(-20.9012891548179,25.3859202673106,-36.9408958021572));
#23867=CARTESIAN_POINT('Ctrl Pts',(-20.7214655696302,25.1222917104592,-36.9614576145724));
#23868=CARTESIAN_POINT('Ctrl Pts',(-20.5893874971589,24.8566079250204,-36.9817484269859));
#23869=CARTESIAN_POINT('Ctrl Pts',(-20.4687214864829,24.4974972777398,-37.0071034550484));
#23870=CARTESIAN_POINT('Ctrl Pts',(-20.4451857494766,24.4172407694423,-37.0126334082737));
#23871=CARTESIAN_POINT('Ctrl Pts',(-20.4176239439082,24.307630086382,-37.0199273645475));
#23872=CARTESIAN_POINT('Ctrl Pts',(-20.4108420365341,24.2790079858269,-37.0218084847883));
#23873=CARTESIAN_POINT('Ctrl Pts',(-20.4021474901377,24.2399371179548,-37.0243407628174));
#23874=CARTESIAN_POINT('Ctrl Pts',(-20.3998934591274,24.2295668200619,-37.0250094950629));
#23875=CARTESIAN_POINT('Ctrl Pts',(-20.3966512292315,24.2142867663075,-37.0259896566054));
#23876=CARTESIAN_POINT('Ctrl Pts',(-20.3956232110241,24.2093856666493,-37.026303262367));
#23877=CARTESIAN_POINT('Ctrl Pts',(-20.3940162371474,24.2016345034524,-37.0267979766154));
#23878=CARTESIAN_POINT('Ctrl Pts',(-20.3934297137064,24.1987860436546,-37.0269795099188));
#23879=CARTESIAN_POINT('Ctrl Pts',(-20.3923284321414,24.19340076058,-37.0273222038245));
#23880=CARTESIAN_POINT('Ctrl Pts',(-20.3918128736046,24.190864106032,-37.0274834099621));
#23881=CARTESIAN_POINT('Ctrl Pts',(-20.3909285335232,24.186485951242,-37.027761271306));
#23882=CARTESIAN_POINT('Ctrl Pts',(-20.3905583049911,24.1846447474206,-37.0278780101468));
#23883=CARTESIAN_POINT('Ctrl Pts',(-20.3898459058394,24.1810857818507,-37.0281034397636));
#23884=CARTESIAN_POINT('Ctrl Pts',(-20.3895035265542,24.1793680670233,-37.0282121426025));
#23885=CARTESIAN_POINT('Ctrl Pts',(-20.3887014777102,24.175327011045,-37.0284676421757));
#23886=CARTESIAN_POINT('Ctrl Pts',(-20.3882429678253,24.1730034367669,-37.0286143718853));
#23887=CARTESIAN_POINT('Ctrl Pts',(-20.3868997885128,24.1661569270317,-37.0290461912863));
#23888=CARTESIAN_POINT('Ctrl Pts',(-20.3860222543053,24.1616325724779,-37.0293308731611));
#23889=CARTESIAN_POINT('Ctrl Pts',(-20.3785932946037,24.1228861942835,-37.0317632144203));
#23890=CARTESIAN_POINT('Ctrl Pts',(-20.372587238311,24.088560206377,-37.0338802718932));
#23891=CARTESIAN_POINT('Ctrl Pts',(-20.3347577116185,23.8495877274757,-37.048399557004));
#23892=CARTESIAN_POINT('Ctrl Pts',(-20.3221651414928,23.6423594290496,-37.0598975835856));
#23893=CARTESIAN_POINT('Ctrl Pts',(-20.3349756002533,23.2833358887545,-37.0799720134211));
#23894=CARTESIAN_POINT('Ctrl Pts',(-20.3511520747039,23.1319197036788,-37.0884843540948));
#23895=CARTESIAN_POINT('Ctrl Pts',(-20.3965823436478,22.878204972137,-37.1033839675376));
#23896=CARTESIAN_POINT('Ctrl Pts',(-20.4203099630275,22.7751786292987,-37.1096149271084));
#23897=CARTESIAN_POINT('Ctrl Pts',(-20.4540633652893,22.6557865073395,-37.1171285287607));
#23898=CARTESIAN_POINT('Ctrl Pts',(-20.4592259924193,22.6381057592781,-37.1182488031723));
#23899=CARTESIAN_POINT('Ctrl Pts',(-20.4662058109562,22.6149414965673,-37.1197268194982));
#23900=CARTESIAN_POINT('Ctrl Pts',(-20.4678866557682,22.6094169911422,-37.1200800879395));
#23901=CARTESIAN_POINT('Ctrl Pts',(-20.4706542902299,22.6004075129069,-37.1206574779322));
#23902=CARTESIAN_POINT('Ctrl Pts',(-20.4717321743401,22.5969197997859,-37.1208813066544));
#23903=CARTESIAN_POINT('Ctrl Pts',(-20.4738207054707,22.5902024114755,-37.1213130084052));
#23904=CARTESIAN_POINT('Ctrl Pts',(-20.4748305187923,22.5869724804359,-37.1215208537655));
#23905=CARTESIAN_POINT('Ctrl Pts',(-20.4771571080245,22.5795717349568,-37.1219977112859));
#23906=CARTESIAN_POINT('Ctrl Pts',(-20.4784772887738,22.575402005298,-37.122266835296));
#23907=CARTESIAN_POINT('Ctrl Pts',(-20.482664822148,22.5622688416679,-37.1231159161463));
#23908=CARTESIAN_POINT('Ctrl Pts',(-20.4855629311026,22.5533153338082,-37.1236968863837));
#23909=CARTESIAN_POINT('Ctrl Pts',(-20.509813297564,22.4795005864367,-37.1285041820101));
#23910=CARTESIAN_POINT('Ctrl Pts',(-20.5331814425093,22.4153246243153,-37.1327969966594));
#23911=CARTESIAN_POINT('Ctrl Pts',(-20.5631375081219,22.340536707713,-37.1379405398788));
#23912=CARTESIAN_POINT('Ctrl Pts',(-20.5677713972584,22.3291567880818,-37.1387270915316));
#23913=CARTESIAN_POINT('Ctrl Pts',(-20.6719243465873,22.0775075340091,-37.1562071435215));
#23914=CARTESIAN_POINT('Ctrl Pts',(-20.8000870842649,21.8501649807577,-37.1738716044171));
#23915=CARTESIAN_POINT('Ctrl Pts',(-21.0511495958757,21.508827937758,-37.2024815974632));
#23916=CARTESIAN_POINT('Ctrl Pts',(-21.1580960415551,21.3844890403788,-37.213422487203));
#23917=CARTESIAN_POINT('Ctrl Pts',(-21.2791325551319,21.263730442552,-37.2241881177271));
#23918=CARTESIAN_POINT('Ctrl Pts',(-21.2842372243073,21.2586714528152,-37.2246393831163));
#23919=CARTESIAN_POINT('Ctrl Pts',(-21.2920419346938,21.2509881628283,-37.2253250684331));
#23920=CARTESIAN_POINT('Ctrl Pts',(-21.2947296816396,21.2483514887378,-37.2255604347402));
#23921=CARTESIAN_POINT('Ctrl Pts',(-21.2991336031428,21.2440463698745,-37.2259448253721));
#23922=CARTESIAN_POINT('Ctrl Pts',(-21.3008470171249,21.2423751254155,-37.2260940674365));
#23923=CARTESIAN_POINT('Ctrl Pts',(-21.3041536115529,21.2391570913953,-37.2263814770422));
#23924=CARTESIAN_POINT('Ctrl Pts',(-21.3057465310845,21.2376100373754,-37.2265196653597));
#23925=CARTESIAN_POINT('Ctrl Pts',(-21.3086508620539,21.2347951590987,-37.2267711300451));
#23926=CARTESIAN_POINT('Ctrl Pts',(-21.3099617461334,21.2335268064907,-37.2268844481109));
#23927=CARTESIAN_POINT('Ctrl Pts',(-21.3126352302189,21.2309444543032,-37.2271151846351));
#23928=CARTESIAN_POINT('Ctrl Pts',(-21.3139979059482,21.2296305472711,-37.2272325958903));
#23929=CARTESIAN_POINT('Ctrl Pts',(-21.3179077626614,21.2258672619489,-37.2275689216671));
#23930=CARTESIAN_POINT('Ctrl Pts',(-21.3204578258751,21.223420861757,-37.2277876022259));
#23931=CARTESIAN_POINT('Ctrl Pts',(-21.3315364505952,21.2128275334951,-37.2287347499183));
#23932=CARTESIAN_POINT('Ctrl Pts',(-21.3401058165719,21.2047231290821,-37.2294599389173));
#23933=CARTESIAN_POINT('Ctrl Pts',(-21.3516495521591,21.1939251783085,-37.2304272415321));
#23934=CARTESIAN_POINT('Ctrl Pts',(-21.3545845990371,21.1911900086105,-37.2306723585473));
#23935=CARTESIAN_POINT('Ctrl Pts',(-21.3635012406099,21.1829116480487,-37.2314145548947));
#23936=CARTESIAN_POINT('Ctrl Pts',(-21.3694988274484,21.1773856258219,-37.2319104225743));
#23937=CARTESIAN_POINT('Ctrl Pts',(-21.3793320306121,21.1683943372869,-37.2327180764042));
#23938=CARTESIAN_POINT('Ctrl Pts',(-21.3831550784082,21.164915467676,-37.2330307768298));
#23939=CARTESIAN_POINT('Ctrl Pts',(-21.3905102723815,21.1582547190517,-37.2336299182521));
#23940=CARTESIAN_POINT('Ctrl Pts',(-21.3940411179842,21.1550714315876,-37.2339164508576));
#23941=CARTESIAN_POINT('Ctrl Pts',(-21.6292109496368,20.943991948395,-37.252929894876));
#23942=CARTESIAN_POINT('Ctrl Pts',(-21.8897738431502,20.7707073969846,-37.2695640823201));
#23943=CARTESIAN_POINT('Ctrl Pts',(-22.2796787110397,20.5861051857925,-37.2940671947847));
#23944=CARTESIAN_POINT('Ctrl Pts',(-22.3909488960132,20.5408442685849,-37.3010027472906));
#23945=CARTESIAN_POINT('Ctrl Pts',(-22.5535652106443,20.4850567430032,-37.3112328660317));
#23946=CARTESIAN_POINT('Ctrl Pts',(-22.6030509572489,20.469405319842,-37.3143572633185));
#23947=CARTESIAN_POINT('Ctrl Pts',(-22.660579327027,20.4527271918678,-37.3180094928179));
#23948=CARTESIAN_POINT('Ctrl Pts',(-22.6682759339228,20.4505269113965,-37.3184985232653));
#23949=CARTESIAN_POINT('Ctrl Pts',(-22.6799644502443,20.4472324947613,-37.3192418356578));
#23950=CARTESIAN_POINT('Ctrl Pts',(-22.6839504409069,20.4461173249796,-37.3194954313638));
#23951=CARTESIAN_POINT('Ctrl Pts',(-22.6911644731956,20.4441140158997,-37.319954609326));
#23952=CARTESIAN_POINT('Ctrl Pts',(-22.6943917765104,20.4432232207354,-37.3201601047418));
#23953=CARTESIAN_POINT('Ctrl Pts',(-22.7008342218527,20.4414557864781,-37.3205704739989));
#23954=CARTESIAN_POINT('Ctrl Pts',(-22.7040493473421,20.4405791020844,-37.3207753460816));
#23955=CARTESIAN_POINT('Ctrl Pts',(-22.7130653573476,20.4381356793561,-37.321350073915));
#23956=CARTESIAN_POINT('Ctrl Pts',(-22.7188692499781,20.4365801813018,-37.3217202945575));
#23957=CARTESIAN_POINT('Ctrl Pts',(-22.7424998708982,20.430317732764,-37.3232286948233));
#23958=CARTESIAN_POINT('Ctrl Pts',(-22.7603622126316,20.4257476474437,-37.3243713049434));
#23959=CARTESIAN_POINT('Ctrl Pts',(-23.0731096249258,20.3485843510148,-37.3444218304116));
#23960=CARTESIAN_POINT('Ctrl Pts',(-23.3766952589901,20.3178951344871,-37.3648010753388));
#23961=CARTESIAN_POINT('Ctrl Pts',(-23.8709422811502,20.3378085359216,-37.3982708681225));
#23962=CARTESIAN_POINT('Ctrl Pts',(-24.0608554988106,20.362472357072,-37.4111405717495));
#23963=CARTESIAN_POINT('Ctrl Pts',(-24.2531145330685,20.4050759331034,-37.4235129173923));
#23964=CARTESIAN_POINT('Ctrl Pts',(-24.2587423626297,20.4063388894376,-37.4238744730507));
#23965=CARTESIAN_POINT('Ctrl Pts',(-24.267500776313,20.4083291005925,-37.4244361690166));
#23966=CARTESIAN_POINT('Ctrl Pts',(-24.2706336797585,20.4090459334199,-37.4246368930234));
#23967=CARTESIAN_POINT('Ctrl Pts',(-24.2758726339705,20.4102528971005,-37.4249722171388));
#23968=CARTESIAN_POINT('Ctrl Pts',(-24.2779792643693,20.410740461214,-37.4251069636069));
#23969=CARTESIAN_POINT('Ctrl Pts',(-24.2820877060613,20.411695687223,-37.4253695735218));
#23970=CARTESIAN_POINT('Ctrl Pts',(-24.2840895631321,20.4121631448594,-37.4254974486969));
#23971=CARTESIAN_POINT('Ctrl Pts',(-24.2877787718882,20.4130283425664,-37.4257329547294));
#23972=CARTESIAN_POINT('Ctrl Pts',(-24.2894662381035,20.4134255259292,-37.4258406168796));
#23973=CARTESIAN_POINT('Ctrl Pts',(-24.2934200219409,20.4143595060595,-37.4260927334758));
#23974=CARTESIAN_POINT('Ctrl Pts',(-24.2956860759983,20.4148973974385,-37.4262371235293));
#23975=CARTESIAN_POINT('Ctrl Pts',(-24.3014518595442,20.4162726208633,-37.4266042442665));
#23976=CARTESIAN_POINT('Ctrl Pts',(-24.3049507838178,20.4171133614396,-37.4268267777928));
#23977=CARTESIAN_POINT('Ctrl Pts',(-24.3243528887679,20.4218097918628,-37.4280594064011));
#23978=CARTESIAN_POINT('Ctrl Pts',(-24.3402283087102,20.4257807943281,-37.4290629255336));
#23979=CARTESIAN_POINT('Ctrl Pts',(-24.6599465350137,20.5083462381508,-37.4491835003535));
#23980=CARTESIAN_POINT('Ctrl Pts',(-24.9507845281354,20.630800225073,-37.4659750232047));
#23981=CARTESIAN_POINT('Ctrl Pts',(-25.2791100211497,20.829582032101,-37.4876914839827));
#23982=CARTESIAN_POINT('Ctrl Pts',(-25.3376653696716,20.8676883070834,-37.4916784197165));
#23983=CARTESIAN_POINT('Ctrl Pts',(-25.4482144073005,20.9448580635898,-37.4994835176825));
#23984=CARTESIAN_POINT('Ctrl Pts',(-25.5003546619567,20.9836515694298,-37.5032921868166));
#23985=CARTESIAN_POINT('Ctrl Pts',(-25.5914375333036,21.0557976469041,-37.5102086386598));
#23986=CARTESIAN_POINT('Ctrl Pts',(-25.6308247159875,21.0885538675047,-37.5132930721422));
#23987=CARTESIAN_POINT('Ctrl Pts',(-25.6754241823579,21.127480012607,-37.5169027193317));
#23988=CARTESIAN_POINT('Ctrl Pts',(-25.6814158737262,21.1327488539714,-37.5173901594325));
#23989=CARTESIAN_POINT('Ctrl Pts',(-25.6904818669095,21.1407810042118,-37.5181315425866));
#23990=CARTESIAN_POINT('Ctrl Pts',(-25.6935705505238,21.1435280940046,-37.5183848048454));
#23991=CARTESIAN_POINT('Ctrl Pts',(-25.6991510210782,21.1485106531483,-37.5188436249328));
#23992=CARTESIAN_POINT('Ctrl Pts',(-25.7016446301775,21.1507440805139,-37.5190490965428));
#23993=CARTESIAN_POINT('Ctrl Pts',(-25.7066158415379,21.1552105772397,-37.5194596224815));
#23994=CARTESIAN_POINT('Ctrl Pts',(-25.7090934660444,21.1574436158633,-37.5196646753754));
#23995=CARTESIAN_POINT('Ctrl Pts',(-25.7160355338494,21.1637199361649,-37.5202404788553));
#23996=CARTESIAN_POINT('Ctrl Pts',(-25.7204920978669,21.1677718777164,-37.5206115965965));
#23997=CARTESIAN_POINT('Ctrl Pts',(-25.7386263407493,21.1843527687509,-37.5221277616929));
#23998=CARTESIAN_POINT('Ctrl Pts',(-25.7522068783411,21.1969870029921,-37.5232772968109));
#23999=CARTESIAN_POINT('Ctrl Pts',(-26.0535389158611,21.4822141807541,-37.5491051998075));
#24000=CARTESIAN_POINT('Ctrl Pts',(-26.2886177969138,21.8054348717724,-37.5764952710242));
#24001=CARTESIAN_POINT('Ctrl Pts',(-26.4910984623381,22.2300038847135,-37.6077460902152));
#24002=CARTESIAN_POINT('Ctrl Pts',(-26.5207388614044,22.2981167620192,-37.61261279651));
#24003=CARTESIAN_POINT('Ctrl Pts',(-26.559157874808,22.3954669239625,-37.6193071854443));
#24004=CARTESIAN_POINT('Ctrl Pts',(-26.5699142628081,22.423893637066,-37.6212312972315));
#24005=CARTESIAN_POINT('Ctrl Pts',(-26.5818072552407,22.4567197446316,-37.6234146595572));
#24006=CARTESIAN_POINT('Ctrl Pts',(-26.58333819552,22.4609732494497,-37.623696834542));
#24007=CARTESIAN_POINT('Ctrl Pts',(-26.5856402897465,22.4674117818494,-37.6241228317478));
#24008=CARTESIAN_POINT('Ctrl Pts',(-26.5864180373342,22.4695944203095,-37.6242670468858));
#24009=CARTESIAN_POINT('Ctrl Pts',(-26.5878179878697,22.473536624356,-37.6245271663509));
#24010=CARTESIAN_POINT('Ctrl Pts',(-26.5884410146447,22.4752958870842,-37.62464311992));
#24011=CARTESIAN_POINT('Ctrl Pts',(-26.5897795584501,22.479086040186,-37.6248926535408));
#24012=CARTESIAN_POINT('Ctrl Pts',(-26.5904945664649,22.4811171010828,-37.6250262026329));
#24013=CARTESIAN_POINT('Ctrl Pts',(-26.5924204735578,22.4866054122092,-37.6253866208667));
#24014=CARTESIAN_POINT('Ctrl Pts',(-26.5936275191521,22.4900640261333,-37.6256132594245));
#24015=CARTESIAN_POINT('Ctrl Pts',(-26.5992070193244,22.5061393226923,-37.6266644151307));
#24016=CARTESIAN_POINT('Ctrl Pts',(-26.6035070147381,22.5187812828148,-37.6274846690028));
#24017=CARTESIAN_POINT('Ctrl Pts',(-26.6082170898878,22.532916445135,-37.6283950661363));
#24018=CARTESIAN_POINT('Ctrl Pts',(-26.6087047259833,22.5343833829003,-37.628489465751));
#24019=CARTESIAN_POINT('Ctrl Pts',(-26.717427976832,22.8622394158628,-37.6495695564401));
#24020=CARTESIAN_POINT('Ctrl Pts',(-26.7727528314061,23.2039094479507,-37.6677547064651));
#24021=CARTESIAN_POINT('Ctrl Pts',(-26.7731123298941,23.7008682127994,-37.696099867811));
#24022=CARTESIAN_POINT('Ctrl Pts',(-26.762335296893,23.8536085215606,-37.7050364969116));
#24023=CARTESIAN_POINT('Ctrl Pts',(-26.7391736259298,24.0161129948632,-37.7150203235191));
#24024=CARTESIAN_POINT('Ctrl Pts',(-26.7375306741415,24.0272239711745,-37.715705290494));
#24025=CARTESIAN_POINT('Ctrl Pts',(-26.7351635184718,24.0426740154106,-37.7166610800836));
#24026=CARTESIAN_POINT('Ctrl Pts',(-26.7344884487135,24.0470206222298,-37.7169303423269));
#24027=CARTESIAN_POINT('Ctrl Pts',(-26.733309295666,24.054511732735,-37.7173950373301));
#24028=CARTESIAN_POINT('Ctrl Pts',(-26.7328094450094,24.0576569048535,-37.7175903353991));
#24029=CARTESIAN_POINT('Ctrl Pts',(-26.7317671207605,24.0641533072367,-37.7179941297855));
#24030=CARTESIAN_POINT('Ctrl Pts',(-26.7312240124271,24.0675044298742,-37.7182026460326));
#24031=CARTESIAN_POINT('Ctrl Pts',(-26.7299457291426,24.0753136209977,-37.7186890757952));
#24032=CARTESIAN_POINT('Ctrl Pts',(-26.7292064732751,24.0797710057584,-37.7189671188525));
#24033=CARTESIAN_POINT('Ctrl Pts',(-26.7268138571492,24.0940118141665,-37.7198567055706));
#24034=CARTESIAN_POINT('Ctrl Pts',(-26.7251246999613,24.1037890917161,-37.7204693880731));
#24035=CARTESIAN_POINT('Ctrl Pts',(-26.6897909629276,24.3028263133023,-37.7329815617794));
#24036=CARTESIAN_POINT('Ctrl Pts',(-26.6393321704379,24.4886722524044,-37.7454331150915));
#24037=CARTESIAN_POINT('Ctrl Pts',(-26.4732111835675,24.9375049430528,-37.777372680108));
#24038=CARTESIAN_POINT('Ctrl Pts',(-26.3384312776336,25.1916591337613,-37.7972449007599));
#24039=CARTESIAN_POINT('Ctrl Pts',(-26.1526947013432,25.4514353619639,-37.8177173445063));
#24040=CARTESIAN_POINT('Ctrl Pts',(-26.1331367475636,25.4779223003326,-37.8198050650802));
#24041=CARTESIAN_POINT('Ctrl Pts',(-26.1101240450259,25.5081086880994,-37.8221803551214));
#24042=CARTESIAN_POINT('Ctrl Pts',(-26.1070632748303,25.5121041363126,-37.822494664012));
#24043=CARTESIAN_POINT('Ctrl Pts',(-26.1025164724738,25.5180106975703,-37.8229591704877));
#24044=CARTESIAN_POINT('Ctrl Pts',(-26.1010376455779,25.5199273083154,-37.8231098750125));
#24045=CARTESIAN_POINT('Ctrl Pts',(-26.0984086558008,25.523326643576,-37.8233771246168));
#24046=CARTESIAN_POINT('Ctrl Pts',(-26.0972593579814,25.5248100291394,-37.8234937311626));
#24047=CARTESIAN_POINT('Ctrl Pts',(-26.0948291118705,25.5279410677493,-37.8237398255017));
#24048=CARTESIAN_POINT('Ctrl Pts',(-26.0935478617617,25.5295884764347,-37.8238692908511));
#24049=CARTESIAN_POINT('Ctrl Pts',(-26.0901365341274,25.533965920001,-37.8242132572683));
#24050=CARTESIAN_POINT('Ctrl Pts',(-26.0880036478941,25.5366937780586,-37.8244275576568));
#24051=CARTESIAN_POINT('Ctrl Pts',(-26.0781128578401,25.5493016891547,-37.8254178465574));
#24052=CARTESIAN_POINT('Ctrl Pts',(-26.0703014874354,25.5591399440098,-37.82619005753));
#24053=CARTESIAN_POINT('Ctrl Pts',(-25.8774118333608,25.7991847101451,-37.8450251496007));
#24054=CARTESIAN_POINT('Ctrl Pts',(-25.6615785201261,26.0029525353146,-37.8609634119767));
#24055=CARTESIAN_POINT('Ctrl Pts',(-25.2569468905883,26.2913989095563,-37.8889301948338));
#24056=CARTESIAN_POINT('Ctrl Pts',(-25.0823583613597,26.3926674226764,-37.9005093404163));
#24057=CARTESIAN_POINT('Ctrl Pts',(-24.8875740081073,26.4824634126707,-37.9135385063693));
#24058=CARTESIAN_POINT('Ctrl Pts',(-24.8756368316123,26.4878784151874,-37.9143372345919));
#24059=CARTESIAN_POINT('Ctrl Pts',(-24.8593778119122,26.4951346389228,-37.9154255893999));
#24060=CARTESIAN_POINT('Ctrl Pts',(-24.8550843730841,26.497039509081,-37.9157130279965));
#24061=CARTESIAN_POINT('Ctrl Pts',(-24.8477990294346,26.5002527540713,-37.9162008469323));
#24062=CARTESIAN_POINT('Ctrl Pts',(-24.8448092628699,26.5015659842901,-37.9164010605617));
#24063=CARTESIAN_POINT('Ctrl Pts',(-24.8387990335586,26.5041950378442,-37.9168035898922));
#24064=CARTESIAN_POINT('Ctrl Pts',(-24.8357785393923,26.5055107776877,-37.9170059081121));
#24065=CARTESIAN_POINT('Ctrl Pts',(-24.8289429006226,26.5084759476815,-37.9174638274077));
#24066=CARTESIAN_POINT('Ctrl Pts',(-24.8251265775759,26.5101226311013,-37.9177195219952));
#24067=CARTESIAN_POINT('Ctrl Pts',(-24.8171486007868,26.5135467106708,-37.9182541347397));
#24068=CARTESIAN_POINT('Ctrl Pts',(-24.8129863701936,26.5153227321805,-37.9185330992097));
#24069=CARTESIAN_POINT('Ctrl Pts',(-24.8021080829578,26.5199374316262,-37.9192623275035));
#24070=CARTESIAN_POINT('Ctrl Pts',(-24.7953861369903,26.5227620825069,-37.9197130684312));
#24071=CARTESIAN_POINT('Ctrl Pts',(-24.7754924057297,26.5310423722638,-37.9210474710432));
#24072=CARTESIAN_POINT('Ctrl Pts',(-24.7622940692926,26.5364333907799,-37.9219333208787));
#24073=CARTESIAN_POINT('Ctrl Pts',(-24.6215405100037,26.5928390056621,-37.9313870326363));
#24074=CARTESIAN_POINT('Ctrl Pts',(-24.4909010189325,26.6357284812981,-37.9402280687868));
#24075=CARTESIAN_POINT('Ctrl Pts',(-24.193664843396,26.7126776490549,-37.9604849509993));
#24076=CARTESIAN_POINT('Ctrl Pts',(-24.0262993773536,26.7421615604559,-37.9719922135855));
#24077=CARTESIAN_POINT('Ctrl Pts',(-23.7312699386574,26.7704088236321,-37.9920375896965));
#24078=CARTESIAN_POINT('Ctrl Pts',(-23.6045213776598,26.7750367690352,-38.0005672642319));
#24079=CARTESIAN_POINT('Ctrl Pts',(-23.4736576171515,26.7720948819442,-38.0091046607864));
#24080=CARTESIAN_POINT('Ctrl Pts',(-23.4694937060768,26.7719931983542,-38.0093760227726));
#24081=CARTESIAN_POINT('Ctrl Pts',(-23.4547782165255,26.7716052964206,-38.010333991924));
#24082=CARTESIAN_POINT('Ctrl Pts',(-23.4442277450624,26.7712753086864,-38.0110189331095));
#24083=CARTESIAN_POINT('Ctrl Pts',(-23.4273732920593,26.7706652487915,-38.0121099220112));
#24084=CARTESIAN_POINT('Ctrl Pts',(-23.4210682641499,26.7704184904986,-38.0125173286109));
#24085=CARTESIAN_POINT('Ctrl Pts',(-23.3742217693644,26.7684472604301,-38.015538839341));
#24086=CARTESIAN_POINT('Ctrl Pts',(-23.3337130194319,26.7659756484109,-38.0181208296042));
#24087=CARTESIAN_POINT('Ctrl Pts',(-23.2879964020829,26.7623184031118,-38.0209919059351));
#24088=CARTESIAN_POINT('Ctrl Pts',(-23.2827343142593,26.7618844290524,-38.0213217301709));
#24089=CARTESIAN_POINT('Ctrl Pts',(-23.2750020254963,26.7612275973817,-38.0218054156971));
#24090=CARTESIAN_POINT('Ctrl Pts',(-23.272531011789,26.7610148198604,-38.0219598419226));
#24091=CARTESIAN_POINT('Ctrl Pts',(-23.2681764252666,26.7606347843948,-38.0222317227072));
#24092=CARTESIAN_POINT('Ctrl Pts',(-23.2662927522785,26.7604687209907,-38.022349245116));
#24093=CARTESIAN_POINT('Ctrl Pts',(-23.2623793743014,26.7601202486994,-38.0225932217337));
#24094=CARTESIAN_POINT('Ctrl Pts',(-23.2603496997557,26.759937572864,-38.0227196603866));
#24095=CARTESIAN_POINT('Ctrl Pts',(-23.2550902011703,26.7594591751348,-38.0230470453279));
#24096=CARTESIAN_POINT('Ctrl Pts',(-23.2518606376958,26.7591605016242,-38.0232478241203));
#24097=CARTESIAN_POINT('Ctrl Pts',(-23.2381828866658,26.7578747410101,-38.0240971183542));
#24098=CARTESIAN_POINT('Ctrl Pts',(-23.2277389490282,26.7568414821584,-38.0247430485934));
#24099=CARTESIAN_POINT('Ctrl Pts',(-23.0447221993495,26.737831721578,-38.0360200570815));
#24100=CARTESIAN_POINT('Ctrl Pts',(-22.8738451634382,26.7059955278453,-38.0458992619199));
#24101=CARTESIAN_POINT('Ctrl Pts',(-22.4878650167069,26.6012681101516,-38.0683590644733));
#24102=CARTESIAN_POINT('Ctrl Pts',(-22.2762690101925,26.5191433323991,-38.0808186862156));
#24103=CARTESIAN_POINT('Ctrl Pts',(-22.0750360152969,26.415536774531,-38.0939694478973));
#24104=CARTESIAN_POINT('',(-26.7730018305864,23.5523783233448,-37.9378739682608));
#24105=CARTESIAN_POINT('Ctrl Pts',(-22.0750360565132,26.4155367957515,-38.344122456765));
#24106=CARTESIAN_POINT('Ctrl Pts',(-22.220339252178,26.4903474073303,-38.3348808102299));
#24107=CARTESIAN_POINT('Ctrl Pts',(-22.3711316413935,26.5540020787549,-38.3254440950023));
#24108=CARTESIAN_POINT('Ctrl Pts',(-22.5361980506722,26.6093249462508,-38.314953907139));
#24109=CARTESIAN_POINT('Ctrl Pts',(-22.5462921837423,26.6126525943229,-38.3143118672905));
#24110=CARTESIAN_POINT('Ctrl Pts',(-22.5735065165015,26.6214751021643,-38.3125792932629));
#24111=CARTESIAN_POINT('Ctrl Pts',(-22.5906563584353,26.6268766587861,-38.3114857654085));
#24112=CARTESIAN_POINT('Ctrl Pts',(-22.613538704027,26.6338738041531,-38.3100241665223));
#24113=CARTESIAN_POINT('Ctrl Pts',(-22.6192319465339,26.6355975069218,-38.3096603045723));
#24114=CARTESIAN_POINT('Ctrl Pts',(-22.628110587026,26.6382588176517,-38.3090925237686));
#24115=CARTESIAN_POINT('Ctrl Pts',(-22.6312927374655,26.639207287706,-38.3088889610273));
#24116=CARTESIAN_POINT('Ctrl Pts',(-22.6376503362765,26.6410915366569,-38.3084821278023));
#24117=CARTESIAN_POINT('Ctrl Pts',(-22.6408257721307,26.6420273440861,-38.308278858531));
#24118=CARTESIAN_POINT('Ctrl Pts',(-22.6478994578794,26.6441001332727,-38.307825896811));
#24119=CARTESIAN_POINT('Ctrl Pts',(-22.6517984211596,26.6452346419234,-38.3075761238706));
#24120=CARTESIAN_POINT('Ctrl Pts',(-22.6630936235026,26.648498143519,-38.3068522314727));
#24121=CARTESIAN_POINT('Ctrl Pts',(-22.6704953203636,26.6506080027717,-38.3063774881166));
#24122=CARTESIAN_POINT('Ctrl Pts',(-22.6872281685213,26.6553129684358,-38.3053033603492));
#24123=CARTESIAN_POINT('Ctrl Pts',(-22.6965635718138,26.6578925564928,-38.3047034741235));
#24124=CARTESIAN_POINT('Ctrl Pts',(-22.7261207255491,26.6659166486943,-38.3028021181087));
#24125=CARTESIAN_POINT('Ctrl Pts',(-22.7463836733696,26.6712060637182,-38.3014956320197));
#24126=CARTESIAN_POINT('Ctrl Pts',(-22.8239776040435,26.6906553051489,-38.2964804445852));
#24127=CARTESIAN_POINT('Ctrl Pts',(-22.8816393937993,26.7034351439089,-38.2927279388175));
#24128=CARTESIAN_POINT('Ctrl Pts',(-23.0531109399128,26.7365243944657,-38.2814888303056));
#24129=CARTESIAN_POINT('Ctrl Pts',(-23.1676902871832,26.7523018245957,-38.2738720218936));
#24130=CARTESIAN_POINT('Ctrl Pts',(-23.5030642062501,26.7802241855337,-38.2513590792522));
#24131=CARTESIAN_POINT('Ctrl Pts',(-23.7245620824923,26.7758621616094,-38.2361799841178));
#24132=CARTESIAN_POINT('Ctrl Pts',(-24.0294572807363,26.7383423510628,-38.2158932899358));
#24133=CARTESIAN_POINT('Ctrl Pts',(-24.1145980491553,26.7243777926618,-38.2103025684005));
#24134=CARTESIAN_POINT('Ctrl Pts',(-24.2053065332842,26.7057338213283,-38.2044975888197));
#24135=CARTESIAN_POINT('Ctrl Pts',(-24.2115250312575,26.7044365144673,-38.2041004039014));
#24136=CARTESIAN_POINT('Ctrl Pts',(-24.2201538743822,26.7026097200451,-38.2035503808946));
#24137=CARTESIAN_POINT('Ctrl Pts',(-24.2225674553539,26.7020958487719,-38.2033966546799));
#24138=CARTESIAN_POINT('Ctrl Pts',(-24.2267183946613,26.7012070946237,-38.2031324836929));
#24139=CARTESIAN_POINT('Ctrl Pts',(-24.2284560326731,26.7008335467931,-38.2030219619794));
#24140=CARTESIAN_POINT('Ctrl Pts',(-24.23204815015,26.7000582237408,-38.2027936200136));
#24141=CARTESIAN_POINT('Ctrl Pts',(-24.2339025804704,26.699656248879,-38.2026758120908));
#24142=CARTESIAN_POINT('Ctrl Pts',(-24.2382612498682,26.6987074124988,-38.2023990863687));
#24143=CARTESIAN_POINT('Ctrl Pts',(-24.2407652002322,26.6981591992185,-38.2022402468497));
#24144=CARTESIAN_POINT('Ctrl Pts',(-24.2489187351671,26.6963638729499,-38.2017234472441));
#24145=CARTESIAN_POINT('Ctrl Pts',(-24.2545656575119,26.6951045246321,-38.2013661897206));
#24146=CARTESIAN_POINT('Ctrl Pts',(-24.441831943373,26.6528116423814,-38.1895397505751));
#24147=CARTESIAN_POINT('Ctrl Pts',(-24.6195908352636,26.5961228276987,-38.1789646639608));
#24148=CARTESIAN_POINT('Ctrl Pts',(-24.8762104082217,26.4890248276558,-38.1633662781439));
#24149=CARTESIAN_POINT('Ctrl Pts',(-24.9593894964257,26.4500594289783,-38.1582561380689));
#24150=CARTESIAN_POINT('Ctrl Pts',(-25.1467671142189,26.3523135034442,-38.1464130241019));
#24151=CARTESIAN_POINT('Ctrl Pts',(-25.2495794807149,26.291181142095,-38.1396630767961));
#24152=CARTESIAN_POINT('Ctrl Pts',(-25.3798380893999,26.2035782744985,-38.1305727889708));
#24153=CARTESIAN_POINT('Ctrl Pts',(-25.410554559422,26.1821334235194,-38.128387861814));
#24154=CARTESIAN_POINT('Ctrl Pts',(-25.4464137455449,26.1561567405847,-38.1257835906815));
#24155=CARTESIAN_POINT('Ctrl Pts',(-25.4519252763339,26.1521373996613,-38.1253817969592));
#24156=CARTESIAN_POINT('Ctrl Pts',(-25.512974411524,26.1073190870485,-38.1209141667691));
#24157=CARTESIAN_POINT('Ctrl Pts',(-25.5671989968098,26.0647688713247,-38.1167877037574));
#24158=CARTESIAN_POINT('Ctrl Pts',(-25.6272480673598,26.0144554752171,-38.1120160278631));
#24159=CARTESIAN_POINT('Ctrl Pts',(-25.634454181825,26.0083636114979,-38.1114399992281));
#24160=CARTESIAN_POINT('Ctrl Pts',(-25.64496483301,25.9993987318965,-38.1105947653059));
#24161=CARTESIAN_POINT('Ctrl Pts',(-25.6482904797533,25.9965504496619,-38.1103265810841));
#24162=CARTESIAN_POINT('Ctrl Pts',(-25.6541767817733,25.9914882374128,-38.1098505724784));
#24163=CARTESIAN_POINT('Ctrl Pts',(-25.6567397781702,25.9892770295706,-38.1096428611134));
#24164=CARTESIAN_POINT('Ctrl Pts',(-25.6616678936001,25.9850117692677,-38.109242606601));
#24165=CARTESIAN_POINT('Ctrl Pts',(-25.6640335119872,25.982958297438,-38.1090500877378));
#24166=CARTESIAN_POINT('Ctrl Pts',(-25.669094474322,25.9785521805244,-38.1086373848275));
#24167=CARTESIAN_POINT('Ctrl Pts',(-25.6717889001209,25.9761984914438,-38.1084171573502));
#24168=CARTESIAN_POINT('Ctrl Pts',(-25.6819706761241,25.9672743657706,-38.1075830288669));
#24169=CARTESIAN_POINT('Ctrl Pts',(-25.6894314081591,25.9606737655461,-38.1069678659395));
#24170=CARTESIAN_POINT('Ctrl Pts',(-25.7641011847868,25.8939927934585,-38.1007709303699));
#24171=CARTESIAN_POINT('Ctrl Pts',(-25.8287858657781,25.831157502303,-38.095072326474));
#24172=CARTESIAN_POINT('Ctrl Pts',(-25.9356691294068,25.7182413207325,-38.085049235901));
#24173=CARTESIAN_POINT('Ctrl Pts',(-25.9791346323418,25.6694312860357,-38.0807806092283));
#24174=CARTESIAN_POINT('Ctrl Pts',(-26.2415279374595,25.3560898226492,-38.0537899634624));
#24175=CARTESIAN_POINT('Ctrl Pts',(-26.4184644611853,25.0593406610344,-38.0297048515405));
#24176=CARTESIAN_POINT('Ctrl Pts',(-26.5459647107448,24.7384570453726,-38.0078817314065));
#24177=CARTESIAN_POINT('Ctrl Pts',(-26.546688852276,24.736629707286,-38.0077575920336));
#24178=CARTESIAN_POINT('Ctrl Pts',(-26.5522039938893,24.7226752378697,-38.0068106524994));
#24179=CARTESIAN_POINT('Ctrl Pts',(-26.5569231225259,24.7105195506874,-38.0059918327726));
#24180=CARTESIAN_POINT('Ctrl Pts',(-26.5628617325031,24.6949431210107,-38.0049506206503));
#24181=CARTESIAN_POINT('Ctrl Pts',(-26.5641493010733,24.6915487272123,-38.0047242070457));
#24182=CARTESIAN_POINT('Ctrl Pts',(-26.5661887303245,24.6861446973871,-38.0043645271752));
#24183=CARTESIAN_POINT('Ctrl Pts',(-26.5669443196199,24.6841364865229,-38.0042310365903));
#24184=CARTESIAN_POINT('Ctrl Pts',(-26.5683536949427,24.6803792579344,-38.0039816069649));
#24185=CARTESIAN_POINT('Ctrl Pts',(-26.5690079620882,24.6786304384514,-38.003865639507));
#24186=CARTESIAN_POINT('Ctrl Pts',(-26.5704744576226,24.6747001734212,-38.0036053090666));
#24187=CARTESIAN_POINT('Ctrl Pts',(-26.5712858409402,24.6725184205782,-38.0034609976653));
#24188=CARTESIAN_POINT('Ctrl Pts',(-26.573683780796,24.6660490834463,-38.0030336789075));
#24189=CARTESIAN_POINT('Ctrl Pts',(-26.5752635871121,24.6617589770909,-38.0027510770052));
#24190=CARTESIAN_POINT('Ctrl Pts',(-26.5877688586537,24.6275756466584,-38.0005053548184));
#24191=CARTESIAN_POINT('Ctrl Pts',(-26.5982605737062,24.5975240786653,-37.9985677765294));
#24192=CARTESIAN_POINT('Ctrl Pts',(-26.6402095798588,24.4713945743225,-37.9905686550977));
#24193=CARTESIAN_POINT('Ctrl Pts',(-26.6675852583896,24.3740108820585,-37.9847117335336));
#24194=CARTESIAN_POINT('Ctrl Pts',(-26.7451118263248,24.0383425423474,-37.9651031045121));
#24195=CARTESIAN_POINT('Ctrl Pts',(-26.7728412889899,23.7957630959875,-37.9518467202304));
#24196=CARTESIAN_POINT('Ctrl Pts',(-26.7730018305864,23.5523783233448,-37.9378739682608));
#24197=CARTESIAN_POINT('Ctrl Pts',(-26.7730018333001,23.5523742052866,-37.9378737318424));
#24198=CARTESIAN_POINT('Ctrl Pts',(-26.7730911924932,23.416640660648,-37.9300812473323));
#24199=CARTESIAN_POINT('Ctrl Pts',(-26.7646056339369,23.2810495026856,-37.922102003823));
#24200=CARTESIAN_POINT('Ctrl Pts',(-26.7467405997613,23.1396085107992,-37.9134215880712));
#24201=CARTESIAN_POINT('Ctrl Pts',(-26.745860591116,23.1328155776368,-37.9130038473182));
#24202=CARTESIAN_POINT('Ctrl Pts',(-26.7443876856687,23.1217236372626,-37.9123203257416));
#24203=CARTESIAN_POINT('Ctrl Pts',(-26.7438077466349,23.1174229069543,-37.9120549547208));
#24204=CARTESIAN_POINT('Ctrl Pts',(-26.7427693146334,23.109837783291,-37.911586308981));
#24205=CARTESIAN_POINT('Ctrl Pts',(-26.7423144346312,23.106552894949,-37.9113831488627));
#24206=CARTESIAN_POINT('Ctrl Pts',(-26.7414109738936,23.1001019072215,-37.9109837726291));
#24207=CARTESIAN_POINT('Ctrl Pts',(-26.7409627493984,23.0969357611553,-37.9107875680176));
#24208=CARTESIAN_POINT('Ctrl Pts',(-26.7400621506442,23.0906416679477,-37.9103971446756));
#24209=CARTESIAN_POINT('Ctrl Pts',(-26.7396098858449,23.0875137083546,-37.9102029296104));
#24210=CARTESIAN_POINT('Ctrl Pts',(-26.7385306499885,23.0801262300063,-37.9097437959496));
#24211=CARTESIAN_POINT('Ctrl Pts',(-26.7378997440641,23.0758672997106,-37.9094787526768));
#24212=CARTESIAN_POINT('Ctrl Pts',(-26.7356735811365,23.0610445602166,-37.9085550726694));
#24213=CARTESIAN_POINT('Ctrl Pts',(-26.7340343438519,23.0504875171673,-37.9078950404987));
#24214=CARTESIAN_POINT('Ctrl Pts',(-26.7132428107517,22.9208407061477,-37.8997623580592));
#24215=CARTESIAN_POINT('Ctrl Pts',(-26.6874741824173,22.802923393408,-37.8920786390624));
#24216=CARTESIAN_POINT('Ctrl Pts',(-26.6500507099806,22.6683609958214,-37.882961914188));
#24217=CARTESIAN_POINT('Ctrl Pts',(-26.6447766435176,22.6500292664898,-37.881712422312));
#24218=CARTESIAN_POINT('Ctrl Pts',(-26.5580415993947,22.3583252216658,-37.8617116604438));
#24219=CARTESIAN_POINT('Ctrl Pts',(-26.4408172739069,22.0969486228799,-37.8419721927852));
#24220=CARTESIAN_POINT('Ctrl Pts',(-26.2529896595378,21.7934152364845,-37.8184328817572));
#24221=CARTESIAN_POINT('Ctrl Pts',(-26.2132055083436,21.7336764983389,-37.8137754473313));
#24222=CARTESIAN_POINT('Ctrl Pts',(-26.1624174854656,21.6626738644952,-37.8082554129752));
#24223=CARTESIAN_POINT('Ctrl Pts',(-26.1532866507094,21.6501019142361,-37.8072786473201));
#24224=CARTESIAN_POINT('Ctrl Pts',(-26.1418545165122,21.6345984429613,-37.8060754089791));
#24225=CARTESIAN_POINT('Ctrl Pts',(-26.1396387911324,21.6316045089557,-37.8058431071608));
#24226=CARTESIAN_POINT('Ctrl Pts',(-26.1361385275616,21.6268919876704,-37.8054775624829));
#24227=CARTESIAN_POINT('Ctrl Pts',(-26.1348574638511,21.6251708423455,-37.8053440771567));
#24228=CARTESIAN_POINT('Ctrl Pts',(-26.1324583157192,21.6219542306148,-37.805094652248));
#24229=CARTESIAN_POINT('Ctrl Pts',(-26.1313406580072,21.6204584667146,-37.8049786842592));
#24230=CARTESIAN_POINT('Ctrl Pts',(-26.1288266872455,21.6171001047736,-37.804718346094));
#24231=CARTESIAN_POINT('Ctrl Pts',(-26.1274296586768,21.6152380517389,-37.8045740275124));
#24232=CARTESIAN_POINT('Ctrl Pts',(-26.1238702850407,21.6105045730915,-37.8042072220258));
#24233=CARTESIAN_POINT('Ctrl Pts',(-26.1217051447657,21.6076352399307,-37.8039849316785));
#24234=CARTESIAN_POINT('Ctrl Pts',(-26.109958055491,21.5921215640767,-37.8027833554382));
#24235=CARTESIAN_POINT('Ctrl Pts',(-26.1002874195711,21.5795441946163,-37.8018102309805));
#24236=CARTESIAN_POINT('Ctrl Pts',(-25.8916731374845,21.3123330410741,-37.7811455902863));
#24237=CARTESIAN_POINT('Ctrl Pts',(-25.6556096173356,21.0889339852216,-37.7639195264112));
#24238=CARTESIAN_POINT('Ctrl Pts',(-25.3274488139758,20.8607294092138,-37.7412507108422));
#24239=CARTESIAN_POINT('Ctrl Pts',(-25.2631581742556,20.8193342779402,-37.7368701272085));
#24240=CARTESIAN_POINT('Ctrl Pts',(-25.1398520844474,20.746008790555,-37.7285136863625));
#24241=CARTESIAN_POINT('Ctrl Pts',(-25.0811934317816,20.713559256619,-37.7245566707447));
#24242=CARTESIAN_POINT('Ctrl Pts',(-24.9903287363559,20.6669330915358,-37.718428289608));
#24243=CARTESIAN_POINT('Ctrl Pts',(-24.9588299135796,20.6514148199631,-37.7163041616954));
#24244=CARTESIAN_POINT('Ctrl Pts',(-24.9206037007261,20.633352358851,-37.7137245964049));
#24245=CARTESIAN_POINT('Ctrl Pts',(-24.9141124910627,20.6303116153877,-37.7132864999427));
#24246=CARTESIAN_POINT('Ctrl Pts',(-24.9046422456555,20.6259138404689,-37.7126472412767));
#24247=CARTESIAN_POINT('Ctrl Pts',(-24.901671169247,20.6245396366494,-37.712446673268));
#24248=CARTESIAN_POINT('Ctrl Pts',(-24.8957597525138,20.6218163710761,-37.7120475800729));
#24249=CARTESIAN_POINT('Ctrl Pts',(-24.8928194641838,20.6204672051293,-37.7118490587729));
#24250=CARTESIAN_POINT('Ctrl Pts',(-24.8869523147816,20.6177857213099,-37.7114528892212));
#24251=CARTESIAN_POINT('Ctrl Pts',(-24.8840254807978,20.6164533524346,-37.7112552429972));
#24252=CARTESIAN_POINT('Ctrl Pts',(-24.8769844030212,20.6132607898822,-37.7107797235714));
#24253=CARTESIAN_POINT('Ctrl Pts',(-24.8728682424817,20.6114048610719,-37.7105017038119));
#24254=CARTESIAN_POINT('Ctrl Pts',(-24.8602557659334,20.6057499066467,-37.7096496988535));
#24255=CARTESIAN_POINT('Ctrl Pts',(-24.8517469384179,20.6019790557464,-37.7090747468707));
#24256=CARTESIAN_POINT('Ctrl Pts',(-24.7543411964697,20.5593156641087,-37.7024908544431));
#24257=CARTESIAN_POINT('Ctrl Pts',(-24.6637563863077,20.5244239263854,-37.6963460408941));
#24258=CARTESIAN_POINT('Ctrl Pts',(-24.4685154243611,20.4591755513086,-37.6830358744338));
#24259=CARTESIAN_POINT('Ctrl Pts',(-24.3636153366538,20.4299318959456,-37.6758452508028));
#24260=CARTESIAN_POINT('Ctrl Pts',(-23.9698542146281,20.3413672663898,-37.6488175042016));
#24261=CARTESIAN_POINT('Ctrl Pts',(-23.6747481804493,20.3164432459355,-37.6283569729549));
#24262=CARTESIAN_POINT('Ctrl Pts',(-23.367525399613,20.3326612552132,-37.608949201336));
#24263=CARTESIAN_POINT('Ctrl Pts',(-23.3546916501153,20.3334157652203,-37.6081421956051));
#24264=CARTESIAN_POINT('Ctrl Pts',(-23.3383785854944,20.3344728156572,-37.6071214357889));
#24265=CARTESIAN_POINT('Ctrl Pts',(-23.3348950160892,20.3347042282315,-37.6069037497585));
#24266=CARTESIAN_POINT('Ctrl Pts',(-23.3293231852453,20.3350834585444,-37.6065560440157));
#24267=CARTESIAN_POINT('Ctrl Pts',(-23.3272346923707,20.3352276502251,-37.606425819899));
#24268=CARTESIAN_POINT('Ctrl Pts',(-23.3234710161034,20.3354911832986,-37.6061913368474));
#24269=CARTESIAN_POINT('Ctrl Pts',(-23.3217957972366,20.3356097982869,-37.6060870375014));
#24270=CARTESIAN_POINT('Ctrl Pts',(-23.3178166874997,20.3358946679321,-37.6058394617778));
#24271=CARTESIAN_POINT('Ctrl Pts',(-23.3155128844092,20.3360620899066,-37.6056962523213));
#24272=CARTESIAN_POINT('Ctrl Pts',(-23.3096820062453,20.3364921339764,-37.6053341181821));
#24273=CARTESIAN_POINT('Ctrl Pts',(-23.3061551695585,20.3367580864327,-37.6051153815033));
#24274=CARTESIAN_POINT('Ctrl Pts',(-23.2870725623711,20.3382286683548,-37.6039334660248));
#24275=CARTESIAN_POINT('Ctrl Pts',(-23.2715249070147,20.339540472148,-37.602976248949));
#24276=CARTESIAN_POINT('Ctrl Pts',(-23.2494973994386,20.3415602151536,-37.6016274770452));
#24277=CARTESIAN_POINT('Ctrl Pts',(-23.2430095342069,20.3421749494169,-37.6012311265864));
#24278=CARTESIAN_POINT('Ctrl Pts',(-23.2298265175743,20.3434644172591,-37.60042753084));
#24279=CARTESIAN_POINT('Ctrl Pts',(-23.2231315240253,20.3441404485936,-37.6000203527169));
#24280=CARTESIAN_POINT('Ctrl Pts',(-23.2134295765215,20.3451508153668,-37.5994315787618));
#24281=CARTESIAN_POINT('Ctrl Pts',(-23.2104209476566,20.3454684188755,-37.5992491754425));
#24282=CARTESIAN_POINT('Ctrl Pts',(-22.952987816507,20.3730107360728,-37.5836568122294));
#24283=CARTESIAN_POINT('Ctrl Pts',(-22.7026704144217,20.4304391031466,-37.5696942306749));
#24284=CARTESIAN_POINT('Ctrl Pts',(-22.3523547669669,20.5561469630578,-37.5488180481327));
#24285=CARTESIAN_POINT('Ctrl Pts',(-22.2451638950221,20.6012920069948,-37.5422426250867));
#24286=CARTESIAN_POINT('Ctrl Pts',(-22.0733034872909,20.6848820877628,-37.5311612219253));
#24287=CARTESIAN_POINT('Ctrl Pts',(-22.0071224250281,20.7199743683063,-37.5267553135996));
#24288=CARTESIAN_POINT('Ctrl Pts',(-21.9204824229074,20.7698575015982,-37.5207659244494));
#24289=CARTESIAN_POINT('Ctrl Pts',(-21.8988852029996,20.7826302629006,-37.5192540037917));
#24290=CARTESIAN_POINT('Ctrl Pts',(-21.8679709681075,20.8014038587516,-37.5170613959897));
#24291=CARTESIAN_POINT('Ctrl Pts',(-21.8585319620951,20.8072028063799,-37.5163880570586));
#24292=CARTESIAN_POINT('Ctrl Pts',(-21.8418169273968,20.8175909450668,-37.5151886833604));
#24293=CARTESIAN_POINT('Ctrl Pts',(-21.834528987411,20.8221608399814,-37.5146633618816));
#24294=CARTESIAN_POINT('Ctrl Pts',(-21.8236729171408,20.8290288347158,-37.5138772479634));
#24295=CARTESIAN_POINT('Ctrl Pts',(-21.8200908471788,20.8313049191886,-37.5136172737665));
#24296=CARTESIAN_POINT('Ctrl Pts',(-21.8137847283613,20.8353294005856,-37.5131585554059));
#24297=CARTESIAN_POINT('Ctrl Pts',(-21.8110587924965,20.8370748417425,-37.5129599216046));
#24298=CARTESIAN_POINT('Ctrl Pts',(-21.8056276915693,20.840563972447,-37.5125634779765));
#24299=CARTESIAN_POINT('Ctrl Pts',(-21.8029224995125,20.842307613605,-37.5123656701036));
#24300=CARTESIAN_POINT('Ctrl Pts',(-21.7964202985438,20.8465124304327,-37.5118893925015));
#24301=CARTESIAN_POINT('Ctrl Pts',(-21.7926258596277,20.8489775515186,-37.5116107751841));
#24302=CARTESIAN_POINT('Ctrl Pts',(-21.781009828686,20.8565589385068,-37.5107557406637));
#24303=CARTESIAN_POINT('Ctrl Pts',(-21.7732053434902,20.8617012109886,-37.5101783472467));
#24304=CARTESIAN_POINT('Ctrl Pts',(-21.6832618142842,20.9215265496103,-37.5034900219499));
#24305=CARTESIAN_POINT('Ctrl Pts',(-21.6036617103341,20.9799149353121,-37.497238512054));
#24306=CARTESIAN_POINT('Ctrl Pts',(-21.3005672212918,21.2244041971574,-37.4720426621432));
#24307=CARTESIAN_POINT('Ctrl Pts',(-21.1000259739087,21.4367260775146,-37.4520412058787));
#24308=CARTESIAN_POINT('Ctrl Pts',(-20.9033981251815,21.7111010955547,-37.4294856851029));
#24309=CARTESIAN_POINT('Ctrl Pts',(-20.8769183579128,21.7498078666695,-37.4263743093721));
#24310=CARTESIAN_POINT('Ctrl Pts',(-20.8232879092614,21.8319954354808,-37.4199336265357));
#24311=CARTESIAN_POINT('Ctrl Pts',(-20.7963098405424,21.8755753068791,-37.416611719997));
#24312=CARTESIAN_POINT('Ctrl Pts',(-20.7580016842836,21.9408888413386,-37.4117893525362));
#24313=CARTESIAN_POINT('Ctrl Pts',(-20.745862639751,21.9621361301263,-37.4102443515039));
#24314=CARTESIAN_POINT('Ctrl Pts',(-20.7318888418725,21.9872547914026,-37.4084474481515));
#24315=CARTESIAN_POINT('Ctrl Pts',(-20.729818764783,21.9909933514319,-37.4081807681304));
#24316=CARTESIAN_POINT('Ctrl Pts',(-20.7266628173735,21.996719841842,-37.4077734649862));
#24317=CARTESIAN_POINT('Ctrl Pts',(-20.7255716066598,21.9987047995635,-37.4076324991341));
#24318=CARTESIAN_POINT('Ctrl Pts',(-20.7235948133116,22.0023096664916,-37.4073768871936));
#24319=CARTESIAN_POINT('Ctrl Pts',(-20.7227085333588,22.0039291798857,-37.4072621963129));
#24320=CARTESIAN_POINT('Ctrl Pts',(-20.7209128720518,22.0072171259262,-37.4070296436872));
#24321=CARTESIAN_POINT('Ctrl Pts',(-20.720003578197,22.0088855947343,-37.4069117877323));
#24322=CARTESIAN_POINT('Ctrl Pts',(-20.7173905133876,22.0136904316385,-37.4065728246397));
#24323=CARTESIAN_POINT('Ctrl Pts',(-20.7156904695907,22.0168288399285,-37.4063519573378));
#24324=CARTESIAN_POINT('Ctrl Pts',(-20.7082501022682,22.0306189694418,-37.4053837892313));
#24325=CARTESIAN_POINT('Ctrl Pts',(-20.7025644820483,22.0413003272697,-37.4046399481648));
#24326=CARTESIAN_POINT('Ctrl Pts',(-20.6953953128578,22.0549536154031,-37.4036965300417));
#24327=CARTESIAN_POINT('Ctrl Pts',(-20.6938561129204,22.0578959764312,-37.4034936532149));
#24328=CARTESIAN_POINT('Ctrl Pts',(-20.5756865080555,22.2846435989383,-37.3878923976318));
#24329=CARTESIAN_POINT('Ctrl Pts',(-20.4857224821955,22.5214134780311,-37.3740369717105));
#24330=CARTESIAN_POINT('Ctrl Pts',(-20.36947754347,22.9849249398032,-37.3472999912089));
#24331=CARTESIAN_POINT('Ctrl Pts',(-20.3377413117578,23.2086734106484,-37.3345351957606));
#24332=CARTESIAN_POINT('Ctrl Pts',(-20.3289818622113,23.451107263167,-37.3199092343669));
#24333=CARTESIAN_POINT('Ctrl Pts',(-20.3284977884434,23.4683326504266,-37.3188661031795));
#24334=CARTESIAN_POINT('Ctrl Pts',(-20.3279836143102,23.4939421331828,-37.317309100605));
#24335=CARTESIAN_POINT('Ctrl Pts',(-20.3278480428498,23.5023239899203,-37.3167985229184));
#24336=CARTESIAN_POINT('Ctrl Pts',(-20.327661148346,23.5175534479343,-37.3158690091136));
#24337=CARTESIAN_POINT('Ctrl Pts',(-20.3275989441436,23.5244008854489,-37.3154504157493));
#24338=CARTESIAN_POINT('Ctrl Pts',(-20.3275357555449,23.5351163349462,-37.3147943039746));
#24339=CARTESIAN_POINT('Ctrl Pts',(-20.3275199101879,23.5389842665981,-37.3145572523741));
#24340=CARTESIAN_POINT('Ctrl Pts',(-20.3275041154014,23.5458626801855,-37.3141353109646));
#24341=CARTESIAN_POINT('Ctrl Pts',(-20.3275014208047,23.5488731563455,-37.313950507572));
#24342=CARTESIAN_POINT('Ctrl Pts',(-20.3275046447199,23.5552430430979,-37.3135591991931));
#24343=CARTESIAN_POINT('Ctrl Pts',(-20.3275115978042,23.5586024475927,-37.3133526619352));
#24344=CARTESIAN_POINT('Ctrl Pts',(-20.3275461181161,23.568103413846,-37.3127680674434));
#24345=CARTESIAN_POINT('Ctrl Pts',(-20.3275859886088,23.5742448920037,-37.312389624366));
#24346=CARTESIAN_POINT('Ctrl Pts',(-20.3278254997188,23.5998591341043,-37.3108088980295));
#24347=CARTESIAN_POINT('Ctrl Pts',(-20.3281840792349,23.6193296789279,-37.3096016356698));
#24348=CARTESIAN_POINT('Ctrl Pts',(-20.3370226346138,23.9409105053207,-37.289565248298));
#24349=CARTESIAN_POINT('Ctrl Pts',(-20.3877817446493,24.2402902391441,-37.2692818246888));
#24350=CARTESIAN_POINT('Ctrl Pts',(-20.5348091599203,24.7019955607147,-37.2364950397347));
#24351=CARTESIAN_POINT('Ctrl Pts',(-20.6048470078265,24.870863520532,-37.2242045672926));
#24352=CARTESIAN_POINT('Ctrl Pts',(-20.6961365338836,25.0470467393533,-37.2116532244708));
#24353=CARTESIAN_POINT('Ctrl Pts',(-20.7035658090274,25.0611283561654,-37.2106521608968));
#24354=CARTESIAN_POINT('Ctrl Pts',(-20.7128758861987,25.0784624097464,-37.2094230467821));
#24355=CARTESIAN_POINT('Ctrl Pts',(-20.7146582489451,25.0817670512998,-37.2091888660066));
#24356=CARTESIAN_POINT('Ctrl Pts',(-20.7174713754834,25.0869610647491,-37.2088210307773));
#24357=CARTESIAN_POINT('Ctrl Pts',(-20.7184982564737,25.0888525184948,-37.2086871287678));
#24358=CARTESIAN_POINT('Ctrl Pts',(-20.7204192523342,25.0923824411095,-37.208437327933));
#24359=CARTESIAN_POINT('Ctrl Pts',(-20.7213128899545,25.0940211509854,-37.208321399862));
#24360=CARTESIAN_POINT('Ctrl Pts',(-20.7233198567875,25.0976938360824,-37.2080616655897));
#24361=CARTESIAN_POINT('Ctrl Pts',(-20.7244339552934,25.0997273821973,-37.2079179099321));
#24362=CARTESIAN_POINT('Ctrl Pts',(-20.7272666339521,25.1048846085758,-37.2075534769928));
#24363=CARTESIAN_POINT('Ctrl Pts',(-20.7289882096909,25.1080066518915,-37.2073329919028));
#24364=CARTESIAN_POINT('Ctrl Pts',(-20.7384391096953,25.1250786123352,-37.2061280258586));
#24365=CARTESIAN_POINT('Ctrl Pts',(-20.7462668983485,25.1389741867031,-37.2051497817923));
#24366=CARTESIAN_POINT('Ctrl Pts',(-20.8976297148873,25.4030635365318,-37.1865952625104));
#24367=CARTESIAN_POINT('Ctrl Pts',(-21.0740356253437,25.632973971005,-37.1710014150161));
#24368=CARTESIAN_POINT('Ctrl Pts',(-21.3631692652182,25.9202643720146,-37.1480736256099));
#24369=CARTESIAN_POINT('Ctrl Pts',(-21.4521946198288,25.9994236205104,-37.1413004721716));
#24370=CARTESIAN_POINT('Ctrl Pts',(-21.609436713965,26.1243627526132,-37.1295627659001));
#24371=CARTESIAN_POINT('Ctrl Pts',(-21.6753940791134,26.1727920478462,-37.1247006189206));
#24372=CARTESIAN_POINT('Ctrl Pts',(-21.7517958183193,26.2245339023315,-37.1191035305024));
#24373=CARTESIAN_POINT('Ctrl Pts',(-21.7605019365269,26.2303682385762,-37.118466246416));
#24374=CARTESIAN_POINT('Ctrl Pts',(-21.7760918485895,26.2407058572732,-37.1173259087012));
#24375=CARTESIAN_POINT('Ctrl Pts',(-21.7829647471771,26.2452254650116,-37.1168234726104));
#24376=CARTESIAN_POINT('Ctrl Pts',(-21.7933428598706,26.2519933238434,-37.1160651949351));
#24377=CARTESIAN_POINT('Ctrl Pts',(-21.7968352881665,26.2542611989791,-37.1158100888637));
#24378=CARTESIAN_POINT('Ctrl Pts',(-21.8030737032703,26.2582950651831,-37.115354518675));
#24379=CARTESIAN_POINT('Ctrl Pts',(-21.8058180016007,26.2600636675057,-37.1151541524579));
#24380=CARTESIAN_POINT('Ctrl Pts',(-21.8113061893956,26.2635888166979,-37.1147535285637));
#24381=CARTESIAN_POINT('Ctrl Pts',(-21.8140500645629,26.2653453790765,-37.1145532717651));
#24382=CARTESIAN_POINT('Ctrl Pts',(-21.8207330997167,26.2696094228366,-37.1140656151049));
#24383=CARTESIAN_POINT('Ctrl Pts',(-21.8246750467624,26.2721125042369,-37.1137780519711));
#24384=CARTESIAN_POINT('Ctrl Pts',(-21.8395486749748,26.2815117533965,-37.11269331063));
#24385=CARTESIAN_POINT('Ctrl Pts',(-21.8505162550517,26.2883506313925,-37.1118940127062));
#24386=CARTESIAN_POINT('Ctrl Pts',(-21.931184689076,26.3379803060511,-37.1060188005543));
#24387=CARTESIAN_POINT('Ctrl Pts',(-22.0024085419043,26.3781439021406,-37.1008507620103));
#24388=CARTESIAN_POINT('Ctrl Pts',(-22.0750364532454,26.4155370000125,-37.0955933117774));
#24389=CARTESIAN_POINT('Origin',(-23.5502525316942,23.5502525316942,-77.3107734492734));
#24390=CARTESIAN_POINT('',(-22.075035776554,26.4155366516121,-35.5970690335682));
#24391=CARTESIAN_POINT('',(-22.0750360716487,26.4155368035442,-35.8409625058884));
#24392=CARTESIAN_POINT('',(-22.0750360153461,26.4155367745563,-77.3107734492734));
#24393=CARTESIAN_POINT('',(-26.7730022894476,23.5490029715869,-36.4420349701589));
#24394=CARTESIAN_POINT('Ctrl Pts',(-22.075035776554,26.4155366516121,-35.5970690335682));
#24395=CARTESIAN_POINT('Ctrl Pts',(-22.0107532744414,26.3824402394554,-35.6019587179599));
#24396=CARTESIAN_POINT('Ctrl Pts',(-21.9475664300769,26.3471712705029,-35.6068371265654));
#24397=CARTESIAN_POINT('Ctrl Pts',(-21.812752629119,26.2658457728297,-35.6173377908743));
#24398=CARTESIAN_POINT('Ctrl Pts',(-21.7416811243655,26.2190396190175,-35.6229332802173));
#24399=CARTESIAN_POINT('Ctrl Pts',(-21.6697392827418,26.1674646657295,-35.6285977129969));
#24400=CARTESIAN_POINT('Ctrl Pts',(-21.6669422290827,26.1654526652079,-35.6288179420446));
#24401=CARTESIAN_POINT('Ctrl Pts',(-21.6596836161164,26.1602136534026,-35.6293894441198));
#24402=CARTESIAN_POINT('Ctrl Pts',(-21.6552270684156,26.1569796704396,-35.6297403149775));
#24403=CARTESIAN_POINT('Ctrl Pts',(-21.6385285653988,26.1447966128086,-35.6310549001775));
#24404=CARTESIAN_POINT('Ctrl Pts',(-21.6263412904979,26.1357724153682,-35.6320141105692));
#24405=CARTESIAN_POINT('Ctrl Pts',(-21.6068196793789,26.1211029651447,-35.6335495998462));
#24406=CARTESIAN_POINT('Ctrl Pts',(-21.5994453353503,26.1155116785104,-35.6341294081067));
#24407=CARTESIAN_POINT('Ctrl Pts',(-21.5895480491372,26.1079401159358,-35.6349071595911));
#24408=CARTESIAN_POINT('Ctrl Pts',(-21.5870039235966,26.1059877976245,-35.635107044945));
#24409=CARTESIAN_POINT('Ctrl Pts',(-21.5830148951747,26.1029172143605,-35.6354203873788));
#24410=CARTESIAN_POINT('Ctrl Pts',(-21.5815680307641,26.1018015193699,-35.635534026623));
#24411=CARTESIAN_POINT('Ctrl Pts',(-21.5786670675373,26.0995606143909,-35.6357618448728));
#24412=CARTESIAN_POINT('Ctrl Pts',(-21.5772129929577,26.098435398283,-35.6358760215629));
#24413=CARTESIAN_POINT('Ctrl Pts',(-21.5739057803371,26.0958716281792,-35.6361356781596));
#24414=CARTESIAN_POINT('Ctrl Pts',(-21.5720532523937,26.0944322968539,-35.6362811014948));
#24415=CARTESIAN_POINT('Ctrl Pts',(-21.5681752932737,26.0914124998234,-35.6365854772679));
#24416=CARTESIAN_POINT('Ctrl Pts',(-21.5661501756678,26.089831631389,-35.6367444009259));
#24417=CARTESIAN_POINT('Ctrl Pts',(-21.5608313389227,26.0856693401253,-35.6371617437551));
#24418=CARTESIAN_POINT('Ctrl Pts',(-21.5575407402255,26.0830839100785,-35.6374198805694));
#24419=CARTESIAN_POINT('Ctrl Pts',(-21.5477315113824,26.0753458304564,-35.6381892343352));
#24420=CARTESIAN_POINT('Ctrl Pts',(-21.5412277019549,26.0701743243771,-35.6386991423172));
#24421=CARTESIAN_POINT('Ctrl Pts',(-21.3042996221875,25.8802805706437,-35.6572704669888));
#24422=CARTESIAN_POINT('Ctrl Pts',(-21.1002912278067,25.6647484709882,-35.6732061335021));
#24423=CARTESIAN_POINT('Ctrl Pts',(-20.810916755184,25.2599385144847,-35.7012112887636));
#24424=CARTESIAN_POINT('Ctrl Pts',(-20.7091064032451,25.0848067685651,-35.7128337841577));
#24425=CARTESIAN_POINT('Ctrl Pts',(-20.6190949321161,24.8898760992118,-35.7258809176289));
#24426=CARTESIAN_POINT('Ctrl Pts',(-20.6138822602348,24.8784113317043,-35.7266485055955));
#24427=CARTESIAN_POINT('Ctrl Pts',(-20.6068500053658,24.8627008021803,-35.7277007631107));
#24428=CARTESIAN_POINT('Ctrl Pts',(-20.6049721029363,24.8584811395121,-35.7279834269913));
#24429=CARTESIAN_POINT('Ctrl Pts',(-20.6017907348512,24.8512910083547,-35.7284651481662));
#24430=CARTESIAN_POINT('Ctrl Pts',(-20.6004826672937,24.8483225730069,-35.7286640473611));
#24431=CARTESIAN_POINT('Ctrl Pts',(-20.5979607632436,24.84257604678,-35.7290491350927));
#24432=CARTESIAN_POINT('Ctrl Pts',(-20.5967463604463,24.839798207507,-35.7292353039367));
#24433=CARTESIAN_POINT('Ctrl Pts',(-20.5938731506484,24.8332006443605,-35.7296775164491));
#24434=CARTESIAN_POINT('Ctrl Pts',(-20.5922178270948,24.8293794177352,-35.7299336789351));
#24435=CARTESIAN_POINT('Ctrl Pts',(-20.5873541418367,24.818091927156,-35.7306904752169));
#24436=CARTESIAN_POINT('Ctrl Pts',(-20.584166626418,24.8106167655123,-35.7311918197179));
#24437=CARTESIAN_POINT('Ctrl Pts',(-20.559555583198,24.7522900419256,-35.7351050015084));
#24438=CARTESIAN_POINT('Ctrl Pts',(-20.5394141374281,24.7009105901345,-35.7385601412958));
#24439=CARTESIAN_POINT('Ctrl Pts',(-20.4754161374854,24.5244513408863,-35.7504641440356));
#24440=CARTESIAN_POINT('Ctrl Pts',(-20.4379636232018,24.3972073062952,-35.759117948007));
#24441=CARTESIAN_POINT('Ctrl Pts',(-20.3617179822319,24.063471871596,-35.7819213069152));
#24442=CARTESIAN_POINT('Ctrl Pts',(-20.3350759002588,23.8548495147009,-35.796302933041));
#24443=CARTESIAN_POINT('Ctrl Pts',(-20.325566288178,23.5319547208434,-35.8178560890464));
#24444=CARTESIAN_POINT('Ctrl Pts',(-20.3281989534184,23.4186725917476,-35.8252745650799));
#24445=CARTESIAN_POINT('Ctrl Pts',(-20.3373340016874,23.2986111958647,-35.8328292915484));
#24446=CARTESIAN_POINT('Ctrl Pts',(-20.3379010899486,23.2914725877073,-35.8332773110015));
#24447=CARTESIAN_POINT('Ctrl Pts',(-20.3387060279458,23.2817504895048,-35.8338858223845));
#24448=CARTESIAN_POINT('Ctrl Pts',(-20.3389232044211,23.2791653790839,-35.8340474670351));
#24449=CARTESIAN_POINT('Ctrl Pts',(-20.3392973391131,23.2747754990508,-35.8343216893323));
#24450=CARTESIAN_POINT('Ctrl Pts',(-20.3394526975793,23.2729706001473,-35.8344343574221));
#24451=CARTESIAN_POINT('Ctrl Pts',(-20.3397692195624,23.2693292977828,-35.8346615007339));
#24452=CARTESIAN_POINT('Ctrl Pts',(-20.339930435754,23.2674929144211,-35.8347759716679));
#24453=CARTESIAN_POINT('Ctrl Pts',(-20.3402890003258,23.2634484095675,-35.8350279063718));
#24454=CARTESIAN_POINT('Ctrl Pts',(-20.3404870511784,23.2612403566126,-35.8351653296351));
#24455=CARTESIAN_POINT('Ctrl Pts',(-20.340917081729,23.2565009467963,-35.8354600483712));
#24456=CARTESIAN_POINT('Ctrl Pts',(-20.3411497784812,23.2539696542649,-35.8356173032819));
#24457=CARTESIAN_POINT('Ctrl Pts',(-20.3417674504216,23.2473366725673,-35.8360289788639));
#24458=CARTESIAN_POINT('Ctrl Pts',(-20.3421572975742,23.2432354251391,-35.8362831274776));
#24459=CARTESIAN_POINT('Ctrl Pts',(-20.3433401340824,23.2310400962046,-35.8370377099155));
#24460=CARTESIAN_POINT('Ctrl Pts',(-20.3441559062838,23.2229481828873,-35.8375368938698));
#24461=CARTESIAN_POINT('Ctrl Pts',(-20.3471332320261,23.1944947904442,-35.8392871530239));
#24462=CARTESIAN_POINT('Ctrl Pts',(-20.3494582447802,23.1741504183958,-35.8405295716965));
#24463=CARTESIAN_POINT('Ctrl Pts',(-20.3613400889921,23.0782897836147,-35.8463469133889));
#24464=CARTESIAN_POINT('Ctrl Pts',(-20.3733771535952,23.0030998383003,-35.8508020949629));
#24465=CARTESIAN_POINT('Ctrl Pts',(-20.4639258741595,22.5426491677104,-35.8778012663908));
#24466=CARTESIAN_POINT('Ctrl Pts',(-20.6097125958165,22.1740461255419,-35.8986459756614));
#24467=CARTESIAN_POINT('Ctrl Pts',(-20.8284406141648,21.8244993508741,-35.9236004287715));
#24468=CARTESIAN_POINT('Ctrl Pts',(-20.8387412907576,21.8083596184647,-35.9247643901203));
#24469=CARTESIAN_POINT('Ctrl Pts',(-20.8525125137447,21.787200186984,-35.9263062687488));
#24470=CARTESIAN_POINT('Ctrl Pts',(-20.8558545171871,21.7820969635255,-35.9266793698951));
#24471=CARTESIAN_POINT('Ctrl Pts',(-20.8610547556704,21.7742052032874,-35.9272582668279));
#24472=CARTESIAN_POINT('Ctrl Pts',(-20.8629028972423,21.7714100053901,-35.9274636827707));
#24473=CARTESIAN_POINT('Ctrl Pts',(-20.8666049759286,21.7658297812189,-35.9278745204069));
#24474=CARTESIAN_POINT('Ctrl Pts',(-20.8684588971314,21.7630447492958,-35.9280799413335));
#24475=CARTESIAN_POINT('Ctrl Pts',(-20.8725974085051,21.7568486568007,-35.9285377995463));
#24476=CARTESIAN_POINT('Ctrl Pts',(-20.8748841837157,21.7534390690305,-35.9287903192331));
#24477=CARTESIAN_POINT('Ctrl Pts',(-20.8815596025397,21.7435269977569,-35.9295260889908));
#24478=CARTESIAN_POINT('Ctrl Pts',(-20.8859654585306,21.7370361918357,-35.930009991253));
#24479=CARTESIAN_POINT('Ctrl Pts',(-20.9174654049111,21.6909924547873,-35.9334576521994));
#24480=CARTESIAN_POINT('Ctrl Pts',(-20.9454142048388,21.6520341619841,-35.9364539388022));
#24481=CARTESIAN_POINT('Ctrl Pts',(-21.0369911254623,21.5302161579891,-35.9460854020439));
#24482=CARTESIAN_POINT('Ctrl Pts',(-21.1037782166715,21.4498265228752,-35.9528423729644));
#24483=CARTESIAN_POINT('Ctrl Pts',(-21.2031151964104,21.3414344825106,-35.9625313422311));
#24484=CARTESIAN_POINT('Ctrl Pts',(-21.2325043644562,21.3106154901051,-35.9653570535876));
#24485=CARTESIAN_POINT('Ctrl Pts',(-21.2878468837449,21.2548366908736,-35.970600418019));
#24486=CARTESIAN_POINT('Ctrl Pts',(-21.3136248668869,21.2297116904468,-35.9730132153234));
#24487=CARTESIAN_POINT('Ctrl Pts',(-21.53682963324,21.0193357749232,-35.9936416703867));
#24488=CARTESIAN_POINT('Ctrl Pts',(-21.7564614118215,20.8592040068082,-36.0123286391318));
#24489=CARTESIAN_POINT('Ctrl Pts',(-21.9964054539959,20.7268348262275,-36.0296510884112));
#24490=CARTESIAN_POINT('Ctrl Pts',(-21.9992744316147,20.7252578036107,-36.0298577823779));
#24491=CARTESIAN_POINT('Ctrl Pts',(-22.0127806142454,20.7178604876721,-36.0308287980162));
#24492=CARTESIAN_POINT('Ctrl Pts',(-22.0234483972759,20.7120957822807,-36.0315898340349));
#24493=CARTESIAN_POINT('Ctrl Pts',(-22.037300748517,20.7047108919092,-36.0325701699526));
#24494=CARTESIAN_POINT('Ctrl Pts',(-22.0404556446343,20.7030357008068,-36.0327929160674));
#24495=CARTESIAN_POINT('Ctrl Pts',(-22.0452934941549,20.7004771948856,-36.0331336698577));
#24496=CARTESIAN_POINT('Ctrl Pts',(-22.0469744414965,20.6995901247212,-36.0332519169738));
#24497=CARTESIAN_POINT('Ctrl Pts',(-22.0502729060431,20.6978531866265,-36.0334836529248));
#24498=CARTESIAN_POINT('Ctrl Pts',(-22.0518903530655,20.6970032115679,-36.0335971480675));
#24499=CARTESIAN_POINT('Ctrl Pts',(-22.055309555937,20.6952101156397,-36.0338367764709));
#24500=CARTESIAN_POINT('Ctrl Pts',(-22.0571114760069,20.6942673275811,-36.0339628881732));
#24501=CARTESIAN_POINT('Ctrl Pts',(-22.060959238576,20.6922587649265,-36.0342318177175));
#24502=CARTESIAN_POINT('Ctrl Pts',(-22.0630053369255,20.6911934792189,-36.0343746043967));
#24503=CARTESIAN_POINT('Ctrl Pts',(-22.0682108095909,20.6884903891633,-36.0347373126078));
#24504=CARTESIAN_POINT('Ctrl Pts',(-22.0713717664647,20.6868556138711,-36.0349570434245));
#24505=CARTESIAN_POINT('Ctrl Pts',(-22.0804454986702,20.6821819182352,-36.0355863260023));
#24506=CARTESIAN_POINT('Ctrl Pts',(-22.0863650207473,20.679156031187,-36.0359950715101));
#24507=CARTESIAN_POINT('Ctrl Pts',(-22.1061886317833,20.669100026416,-36.0373580797539));
#24508=CARTESIAN_POINT('Ctrl Pts',(-22.1201345843245,20.6621522937717,-36.0383074131655));
#24509=CARTESIAN_POINT('Ctrl Pts',(-22.1783906689232,20.6336551496001,-36.0422357162036));
#24510=CARTESIAN_POINT('Ctrl Pts',(-22.2231439871517,20.6130210558798,-36.0451641767871));
#24511=CARTESIAN_POINT('Ctrl Pts',(-22.3080330336073,20.5762184882778,-36.0505850899094));
#24512=CARTESIAN_POINT('Ctrl Pts',(-22.3480543488825,20.5598165135141,-36.0530864616433));
#24513=CARTESIAN_POINT('Ctrl Pts',(-22.7461404371178,20.4059525856993,-36.0775464195381));
#24514=CARTESIAN_POINT('Ctrl Pts',(-23.1256716661585,20.3326478177814,-36.0979705292624));
#24515=CARTESIAN_POINT('Ctrl Pts',(-23.529044166655,20.3275113198189,-36.1223744024461));
#24516=CARTESIAN_POINT('Ctrl Pts',(-23.5488721469664,20.3274418359398,-36.1235794933329));
#24517=CARTESIAN_POINT('Ctrl Pts',(-23.5748844384185,20.3275907296277,-36.1251680636295));
#24518=CARTESIAN_POINT('Ctrl Pts',(-23.5810695600084,20.3276439406223,-36.1255463533756));
#24519=CARTESIAN_POINT('Ctrl Pts',(-23.5906223516881,20.327753627994,-36.1261314983182));
#24520=CARTESIAN_POINT('Ctrl Pts',(-23.59399017427,20.3277975785257,-36.1263379600673));
#24521=CARTESIAN_POINT('Ctrl Pts',(-23.6007015249633,20.3278956855772,-36.1267497350127));
#24522=CARTESIAN_POINT('Ctrl Pts',(-23.6040450501422,20.3279497666728,-36.1269550455878));
#24523=CARTESIAN_POINT('Ctrl Pts',(-23.6114637722123,20.3280813134312,-36.1274109720261));
#24524=CARTESIAN_POINT('Ctrl Pts',(-23.6155389134977,20.3281613064376,-36.127661666931));
#24525=CARTESIAN_POINT('Ctrl Pts',(-23.6273175819483,20.3284148704984,-36.1283870031222));
#24526=CARTESIAN_POINT('Ctrl Pts',(-23.6350206129404,20.3286083384569,-36.1288622684781));
#24527=CARTESIAN_POINT('Ctrl Pts',(-23.687506291901,20.3301149291335,-36.132106838458));
#24528=CARTESIAN_POINT('Ctrl Pts',(-23.7322561429733,20.3323340845006,-36.1349044716053));
#24529=CARTESIAN_POINT('Ctrl Pts',(-23.8295118432328,20.339192118562,-36.1410566749563));
#24530=CARTESIAN_POINT('Ctrl Pts',(-23.8819787816607,20.3441876668337,-36.1444215667582));
#24531=CARTESIAN_POINT('Ctrl Pts',(-24.039590509736,20.3631045483227,-36.1546703911332));
#24532=CARTESIAN_POINT('Ctrl Pts',(-24.1441866825067,20.3809304203879,-36.1616639437822));
#24533=CARTESIAN_POINT('Ctrl Pts',(-24.2777969106109,20.4105476600026,-36.1708149920407));
#24534=CARTESIAN_POINT('Ctrl Pts',(-24.307789943283,20.4176490584613,-36.1728833657153));
#24535=CARTESIAN_POINT('Ctrl Pts',(-24.3626069429963,20.4314612783026,-36.1766873859001));
#24536=CARTESIAN_POINT('Ctrl Pts',(-24.3874615326543,20.4380411573352,-36.178421201947));
#24537=CARTESIAN_POINT('Ctrl Pts',(-24.4334747499402,20.4508135527225,-36.1816462420641));
#24538=CARTESIAN_POINT('Ctrl Pts',(-24.4546538373334,20.4569271783729,-36.1831367185419));
#24539=CARTESIAN_POINT('Ctrl Pts',(-24.4942109175978,20.4687868373105,-36.1859307478422));
#24540=CARTESIAN_POINT('Ctrl Pts',(-24.5126034469167,20.4744812505075,-36.1872340311218));
#24541=CARTESIAN_POINT('Ctrl Pts',(-24.588862307113,20.4988423364142,-36.1926531725849));
#24542=CARTESIAN_POINT('Ctrl Pts',(-24.6462462659162,20.5189801334397,-36.1967685338156));
#24543=CARTESIAN_POINT('Ctrl Pts',(-24.7535890193624,20.5600969332142,-36.2045067533525));
#24544=CARTESIAN_POINT('Ctrl Pts',(-24.8036569302077,20.5807362393794,-36.208132980153));
#24545=CARTESIAN_POINT('Ctrl Pts',(-24.9408526069044,20.6413804498724,-36.2180779359786));
#24546=CARTESIAN_POINT('Ctrl Pts',(-25.0267605246285,20.6840296390332,-36.2243154452348));
#24547=CARTESIAN_POINT('Ctrl Pts',(-25.1163379353043,20.7335991338964,-36.2307341824454));
#24548=CARTESIAN_POINT('Ctrl Pts',(-25.1220185819203,20.736765133493,-36.2311408527865));
#24549=CARTESIAN_POINT('Ctrl Pts',(-25.1298631362062,20.7411683191897,-36.2317018654794));
#24550=CARTESIAN_POINT('Ctrl Pts',(-25.1320352006461,20.7423908251397,-36.2318571427362));
#24551=CARTESIAN_POINT('Ctrl Pts',(-25.1357594016681,20.744492615025,-36.2321232728048));
#24552=CARTESIAN_POINT('Ctrl Pts',(-25.1373122260006,20.7453706676105,-36.2322342051563));
#24553=CARTESIAN_POINT('Ctrl Pts',(-25.1404239611635,20.7471336257898,-36.2324564394005));
#24554=CARTESIAN_POINT('Ctrl Pts',(-25.141982859173,20.7480185406908,-36.2325677398724));
#24555=CARTESIAN_POINT('Ctrl Pts',(-25.1456527913991,20.7501058433916,-36.2328296852688));
#24556=CARTESIAN_POINT('Ctrl Pts',(-25.1477632107688,20.7513093212995,-36.2329802592536));
#24557=CARTESIAN_POINT('Ctrl Pts',(-25.1543247578681,20.7550609173236,-36.2334482330704));
#24558=CARTESIAN_POINT('Ctrl Pts',(-25.1587711930919,20.7576172915265,-36.2337650994647));
#24559=CARTESIAN_POINT('Ctrl Pts',(-25.1690552434334,20.763562576816,-36.2344974226032));
#24560=CARTESIAN_POINT('Ctrl Pts',(-25.1748883768447,20.766959249141,-36.2349123863569));
#24561=CARTESIAN_POINT('Ctrl Pts',(-25.194429921806,20.7784207850511,-36.2363013194906));
#24562=CARTESIAN_POINT('Ctrl Pts',(-25.2080895502048,20.7865689453835,-36.2372701443971));
#24563=CARTESIAN_POINT('Ctrl Pts',(-25.2648322335758,20.8209888417406,-36.241288529141));
#24564=CARTESIAN_POINT('Ctrl Pts',(-25.307357867116,20.8481708724137,-36.2442852071017));
#24565=CARTESIAN_POINT('Ctrl Pts',(-25.3853745700375,20.9006596492826,-36.2497888798089));
#24566=CARTESIAN_POINT('Ctrl Pts',(-25.4210236781023,20.9257085837828,-36.252306193674));
#24567=CARTESIAN_POINT('Ctrl Pts',(-25.6514857867871,21.0947257802935,-36.2686715727514));
#24568=CARTESIAN_POINT('Ctrl Pts',(-25.8300470098783,21.2595451344025,-36.2818490202066));
#24569=CARTESIAN_POINT('Ctrl Pts',(-26.0247025691532,21.4847535087805,-36.2988437550976));
#24570=CARTESIAN_POINT('Ctrl Pts',(-26.059855527674,21.5276103016235,-36.3020358228998));
#24571=CARTESIAN_POINT('Ctrl Pts',(-26.1529170837994,21.6472293699759,-36.3108678134954));
#24572=CARTESIAN_POINT('Ctrl Pts',(-26.2085193316717,21.7257047127247,-36.316579920768));
#24573=CARTESIAN_POINT('Ctrl Pts',(-26.2660363772201,21.8151043180859,-36.3230506979617));
#24574=CARTESIAN_POINT('Ctrl Pts',(-26.2715043773558,21.823692481319,-36.3236719287236));
#24575=CARTESIAN_POINT('Ctrl Pts',(-26.279159199267,21.8358420132757,-36.3245502871064));
#24576=CARTESIAN_POINT('Ctrl Pts',(-26.2813799692715,21.8393820089977,-36.324806155445));
#24577=CARTESIAN_POINT('Ctrl Pts',(-26.2852512800227,21.8455797779992,-36.3252540287319));
#24578=CARTESIAN_POINT('Ctrl Pts',(-26.2869048514074,21.8482356600234,-36.3254459213565));
#24579=CARTESIAN_POINT('Ctrl Pts',(-26.2903662573083,21.853813279013,-36.3258488521215));
#24580=CARTESIAN_POINT('Ctrl Pts',(-26.2921732909445,21.8567355057433,-36.3260599194598));
#24581=CARTESIAN_POINT('Ctrl Pts',(-26.2964695625054,21.8637080810914,-36.3265634532502));
#24582=CARTESIAN_POINT('Ctrl Pts',(-26.2989545125176,21.8677610504655,-36.3268560770918));
#24583=CARTESIAN_POINT('Ctrl Pts',(-26.3072826547232,21.8814119978205,-36.3278414603365));
#24584=CARTESIAN_POINT('Ctrl Pts',(-26.3130845649748,21.8910349517692,-36.3285357324788));
#24585=CARTESIAN_POINT('Ctrl Pts',(-26.3841916826027,22.0103791660734,-36.337142244481));
#24586=CARTESIAN_POINT('Ctrl Pts',(-26.442962298592,22.1238430735884,-36.3452913915235));
#24587=CARTESIAN_POINT('Ctrl Pts',(-26.6279278366797,22.5396774662571,-36.3750807452723));
#24588=CARTESIAN_POINT('Ctrl Pts',(-26.7146150198231,22.8573518750094,-36.3979247463531));
#24589=CARTESIAN_POINT('Ctrl Pts',(-26.753287476269,23.1941353647863,-36.4199456109359));
#24590=CARTESIAN_POINT('Ctrl Pts',(-26.7545493415196,23.2056741589855,-36.4206971687716));
#24591=CARTESIAN_POINT('Ctrl Pts',(-26.7559004212636,23.2186785251735,-36.421540720098));
#24592=CARTESIAN_POINT('Ctrl Pts',(-26.7560509913265,23.2201374760914,-36.4216353084687));
#24593=CARTESIAN_POINT('Ctrl Pts',(-26.7567841785441,23.2272895138481,-36.4220987553971));
#24594=CARTESIAN_POINT('Ctrl Pts',(-26.7573526307428,23.2329840825815,-36.4224670073818));
#24595=CARTESIAN_POINT('Ctrl Pts',(-26.7613538512331,23.2741768529497,-36.4251252510713));
#24596=CARTESIAN_POINT('Ctrl Pts',(-26.7642125082382,23.3097301887667,-36.4273896384842));
#24597=CARTESIAN_POINT('Ctrl Pts',(-26.7667755798403,23.3499563128329,-36.4299123549273));
#24598=CARTESIAN_POINT('Ctrl Pts',(-26.7670606435202,23.3545878520096,-36.4302022265622));
#24599=CARTESIAN_POINT('Ctrl Pts',(-26.7674765760817,23.3615923648447,-36.4306397088367));
#24600=CARTESIAN_POINT('Ctrl Pts',(-26.7676148235739,23.3639648691379,-36.4307877317938));
#24601=CARTESIAN_POINT('Ctrl Pts',(-26.7678505189788,23.368088238524,-36.4310447175752));
#24602=CARTESIAN_POINT('Ctrl Pts',(-26.7679491621894,23.3698390299326,-36.4311537480022));
#24603=CARTESIAN_POINT('Ctrl Pts',(-26.7681446429079,23.3733597251561,-36.4313728243968));
#24604=CARTESIAN_POINT('Ctrl Pts',(-26.7682414491004,23.3751296266156,-36.4314828682035));
#24605=CARTESIAN_POINT('Ctrl Pts',(-26.7684374609901,23.378768346817,-36.4317089248428));
#24606=CARTESIAN_POINT('Ctrl Pts',(-26.7685364993016,23.380637176569,-36.4318249282692));
#24607=CARTESIAN_POINT('Ctrl Pts',(-26.7687633113254,23.3849887897407,-36.432094818453));
#24608=CARTESIAN_POINT('Ctrl Pts',(-26.768889840363,23.3874716410754,-36.4322486350512));
#24609=CARTESIAN_POINT('Ctrl Pts',(-26.7692117558304,23.3939356623409,-36.432648650449));
#24610=CARTESIAN_POINT('Ctrl Pts',(-26.7694026302722,23.3979170679239,-36.4328945977752));
#24611=CARTESIAN_POINT('Ctrl Pts',(-26.7718441184784,23.4508983252572,-36.4361617893169));
#24612=CARTESIAN_POINT('Ctrl Pts',(-26.7729832684713,23.4999458302695,-36.4391218570173));
#24613=CARTESIAN_POINT('Ctrl Pts',(-26.7730022894476,23.5490029715869,-36.4420349701589));
#24614=CARTESIAN_POINT('Ctrl Pts',(-26.7730022880352,23.5489993342442,-36.442034754166));
#24615=CARTESIAN_POINT('Ctrl Pts',(-26.7731226824236,23.8586081559639,-36.4604199725195));
#24616=CARTESIAN_POINT('Ctrl Pts',(-26.7286291185953,24.166677826155,-36.4769583830802));
#24617=CARTESIAN_POINT('Ctrl Pts',(-26.6106445971748,24.5658621958784,-36.5007266761024));
#24618=CARTESIAN_POINT('Ctrl Pts',(-26.5754115693603,24.6664389785736,-36.5069124079058));
#24619=CARTESIAN_POINT('Ctrl Pts',(-26.5170162811,24.8099249044776,-36.5161463037913));
#24620=CARTESIAN_POINT('Ctrl Pts',(-26.497758421538,24.8543500260352,-36.5190639922646));
#24621=CARTESIAN_POINT('Ctrl Pts',(-26.4742180647302,24.9054665298931,-36.5224958313224));
#24622=CARTESIAN_POINT('Ctrl Pts',(-26.4709020715227,24.9125981864629,-36.5229763430071));
#24623=CARTESIAN_POINT('Ctrl Pts',(-26.4658136804945,24.9234377484307,-36.523709316094));
#24624=CARTESIAN_POINT('Ctrl Pts',(-26.4640602241464,24.9271545554474,-36.5239611201872));
#24625=CARTESIAN_POINT('Ctrl Pts',(-26.4608662819037,24.9338913410934,-36.5244183829616));
#24626=CARTESIAN_POINT('Ctrl Pts',(-26.4594281910258,24.9369124542422,-36.5246237581444));
#24627=CARTESIAN_POINT('Ctrl Pts',(-26.4565414703001,24.942952564269,-36.5250349988974));
#24628=CARTESIAN_POINT('Ctrl Pts',(-26.4550928347767,24.9459715538654,-36.5252408644747));
#24629=CARTESIAN_POINT('Ctrl Pts',(-26.4509970218497,24.9544733241031,-36.5258215014578));
#24630=CARTESIAN_POINT('Ctrl Pts',(-26.448339019196,24.9599508473441,-36.5261966502611));
#24631=CARTESIAN_POINT('Ctrl Pts',(-26.4372985426765,24.9825394966469,-36.5277481121702));
#24632=CARTESIAN_POINT('Ctrl Pts',(-26.4287800554097,24.9995833737066,-36.5289291783312));
#24633=CARTESIAN_POINT('Ctrl Pts',(-26.2409413313698,25.367223926891,-36.5546359636457));
#24634=CARTESIAN_POINT('Ctrl Pts',(-25.9990264197442,25.6820380512695,-36.5818310567475));
#24635=CARTESIAN_POINT('Ctrl Pts',(-25.6553338039435,25.9914608353772,-36.6125765604811));
#24636=CARTESIAN_POINT('Ctrl Pts',(-25.6026570842799,26.0359118095854,-36.6171012353082));
#24637=CARTESIAN_POINT('Ctrl Pts',(-25.5290207380977,26.0941110702211,-36.6231335693796));
#24638=CARTESIAN_POINT('Ctrl Pts',(-25.5092696464521,26.1093523558736,-36.6247241166773));
#24639=CARTESIAN_POINT('Ctrl Pts',(-25.4818311405541,26.130021918061,-36.6268939578447));
#24640=CARTESIAN_POINT('Ctrl Pts',(-25.4742945496475,26.1356477292025,-36.6274858839073));
#24641=CARTESIAN_POINT('Ctrl Pts',(-25.4630494465266,26.1439654149974,-36.6283629119021));
#24642=CARTESIAN_POINT('Ctrl Pts',(-25.4593597273105,26.1466824411394,-36.6286496995457));
#24643=CARTESIAN_POINT('Ctrl Pts',(-25.4534593734024,26.1510079515668,-36.629106730802));
#24644=CARTESIAN_POINT('Ctrl Pts',(-25.4512524821438,26.1526214957045,-36.6292773209922));
#24645=CARTESIAN_POINT('Ctrl Pts',(-25.4470517031678,26.1556846537209,-36.6296013637599));
#24646=CARTESIAN_POINT('Ctrl Pts',(-25.445058201822,26.1571347906275,-36.6297548525911));
#24647=CARTESIAN_POINT('Ctrl Pts',(-25.4415612856786,26.1596724293861,-36.6300235901554));
#24648=CARTESIAN_POINT('Ctrl Pts',(-25.4400585941273,26.1607609212289,-36.6301389083117));
#24649=CARTESIAN_POINT('Ctrl Pts',(-25.4371091201912,26.1628935250664,-36.6303649325153));
#24650=CARTESIAN_POINT('Ctrl Pts',(-25.4356624146057,26.163937730654,-36.6304756452222));
#24651=CARTESIAN_POINT('Ctrl Pts',(-25.4321917051512,26.1664384440263,-36.6307408892423));
#24652=CARTESIAN_POINT('Ctrl Pts',(-25.4301668727679,26.1678938078817,-36.6308953405985));
#24653=CARTESIAN_POINT('Ctrl Pts',(-25.4228495316242,26.1731403336719,-36.6314524459631));
#24654=CARTESIAN_POINT('Ctrl Pts',(-25.4175471807539,26.1769178398844,-36.6318541576432));
#24655=CARTESIAN_POINT('Ctrl Pts',(-25.3336242772035,26.2363237280344,-36.6381816288635));
#24656=CARTESIAN_POINT('Ctrl Pts',(-25.2525511894166,26.2884228562152,-36.6438712508975));
#24657=CARTESIAN_POINT('Ctrl Pts',(-25.1302072874201,26.3595051331081,-36.6520411793723));
#24658=CARTESIAN_POINT('Ctrl Pts',(-25.0906835825734,26.3813706203207,-36.6546198534541));
#24659=CARTESIAN_POINT('Ctrl Pts',(-24.9803745014667,26.4394021226365,-36.6616858728934));
#24660=CARTESIAN_POINT('Ctrl Pts',(-24.9086902925355,26.4737917666175,-36.6661328846431));
#24661=CARTESIAN_POINT('Ctrl Pts',(-24.6770562572351,26.5745543578447,-36.6802504920292));
#24662=CARTESIAN_POINT('Ctrl Pts',(-24.5130054242364,26.6307054342304,-36.6898950837052));
#24663=CARTESIAN_POINT('Ctrl Pts',(-24.2731425967293,26.6917623219269,-36.7042158602862));
#24664=CARTESIAN_POINT('Ctrl Pts',(-24.2004264567975,26.7076132126749,-36.7085820788708));
#24665=CARTESIAN_POINT('Ctrl Pts',(-24.0840942168914,26.7287825356893,-36.7156461421667));
#24666=CARTESIAN_POINT('Ctrl Pts',(-24.0408038186365,26.7357507780778,-36.7182918351085));
#24667=CARTESIAN_POINT('Ctrl Pts',(-23.989799781951,26.7428963361587,-36.7214330390408));
#24668=CARTESIAN_POINT('Ctrl Pts',(-23.9822095521032,26.7439321302631,-36.7219011227311));
#24669=CARTESIAN_POINT('Ctrl Pts',(-23.9705847695364,26.745476296607,-36.7226189890103));
#24670=CARTESIAN_POINT('Ctrl Pts',(-23.966552791346,26.7460041164715,-36.7228681554607));
#24671=CARTESIAN_POINT('Ctrl Pts',(-23.9592038132562,26.7469520156586,-36.7233226351609));
#24672=CARTESIAN_POINT('Ctrl Pts',(-23.9558871333161,26.7473745674167,-36.7235278698452));
#24673=CARTESIAN_POINT('Ctrl Pts',(-23.9492223186844,26.7482131403752,-36.7239405344045));
#24674=CARTESIAN_POINT('Ctrl Pts',(-23.9458741764859,26.7486290666945,-36.7241479670068));
#24675=CARTESIAN_POINT('Ctrl Pts',(-23.936357612786,26.7497960995351,-36.7247379228437));
#24676=CARTESIAN_POINT('Ctrl Pts',(-23.9301876883476,26.7505346211404,-36.725120843557));
#24677=CARTESIAN_POINT('Ctrl Pts',(-23.9040895705754,26.7535819522264,-36.7267424105417));
#24678=CARTESIAN_POINT('Ctrl Pts',(-23.884142523074,26.7557224614983,-36.7279863612598));
#24679=CARTESIAN_POINT('Ctrl Pts',(-23.4791881563278,26.7953571162515,-36.7533370871899));
#24680=CARTESIAN_POINT('Ctrl Pts',(-23.0906110243216,26.7633983339045,-36.7800015629711));
#24681=CARTESIAN_POINT('Ctrl Pts',(-22.6511380218023,26.6457945974664,-36.8103056219682));
#24682=CARTESIAN_POINT('Ctrl Pts',(-22.5856972573706,26.6260324265928,-36.8148056323885));
#24683=CARTESIAN_POINT('Ctrl Pts',(-22.4933035148485,26.5948914732856,-36.8210964104967));
#24684=CARTESIAN_POINT('Ctrl Pts',(-22.4658031784721,26.5852051252937,-36.8229606918076));
#24685=CARTESIAN_POINT('Ctrl Pts',(-22.4285404656924,26.5715090213875,-36.8254720875161));
#24686=CARTESIAN_POINT('Ctrl Pts',(-22.4186616794711,26.567822893068,-36.8261364696084));
#24687=CARTESIAN_POINT('Ctrl Pts',(-22.4041401391437,26.5623230464548,-36.8271108126719));
#24688=CARTESIAN_POINT('Ctrl Pts',(-22.399483338135,26.5605469801139,-36.8274229206833));
#24689=CARTESIAN_POINT('Ctrl Pts',(-22.3921247995831,26.5577209222319,-36.827915534507));
#24690=CARTESIAN_POINT('Ctrl Pts',(-22.3894203502868,26.5566780855262,-36.8280964605658));
#24691=CARTESIAN_POINT('Ctrl Pts',(-22.3843084645858,26.5546990143375,-36.8284382068131));
#24692=CARTESIAN_POINT('Ctrl Pts',(-22.3819007421156,26.5537635322724,-36.8285990718142));
#24693=CARTESIAN_POINT('Ctrl Pts',(-22.3777458456606,26.5521434615801,-36.8288764947333));
#24694=CARTESIAN_POINT('Ctrl Pts',(-22.3759981426294,26.5514602408596,-36.8289931357014));
#24695=CARTESIAN_POINT('Ctrl Pts',(-22.372618688603,26.550135724077,-36.8292185744765));
#24696=CARTESIAN_POINT('Ctrl Pts',(-22.3709868664623,26.5494946238196,-36.8293273840237));
#24697=CARTESIAN_POINT('Ctrl Pts',(-22.3671455372906,26.5479818463603,-36.829583413938));
#24698=CARTESIAN_POINT('Ctrl Pts',(-22.3649364655062,26.5471090560438,-36.8297305665844));
#24699=CARTESIAN_POINT('Ctrl Pts',(-22.3584192602511,26.5445258160049,-36.8301644509922));
#24700=CARTESIAN_POINT('Ctrl Pts',(-22.3541138262804,26.5428085037858,-36.8304507693996));
#24701=CARTESIAN_POINT('Ctrl Pts',(-22.3168365836751,26.5278463964645,-36.832927143454));
#24702=CARTESIAN_POINT('Ctrl Pts',(-22.2840805585796,26.5140657705026,-36.8350853630388));
#24703=CARTESIAN_POINT('Ctrl Pts',(-22.1918605764379,26.473460272828,-36.8411290034926));
#24704=CARTESIAN_POINT('Ctrl Pts',(-22.1329934191378,26.4453766498354,-36.8449480597098));
#24705=CARTESIAN_POINT('Ctrl Pts',(-22.0750359454076,26.4155367385478,-36.8487079434683));
#24706=CARTESIAN_POINT('Ctrl Pts',(-22.0750364532454,26.4155370000125,-37.0955933117774));
#24707=CARTESIAN_POINT('Ctrl Pts',(-22.1818001580695,26.4705052014922,-37.0878648110614));
#24708=CARTESIAN_POINT('Ctrl Pts',(-22.2915977141445,26.5194865689918,-37.0799401779364));
#24709=CARTESIAN_POINT('Ctrl Pts',(-22.6793682912363,26.6670676261741,-37.0521550768679));
#24710=CARTESIAN_POINT('Ctrl Pts',(-22.9678889264498,26.7336217801294,-37.0316988392698));
#24711=CARTESIAN_POINT('Ctrl Pts',(-23.2742693173491,26.7611895858928,-37.0122926530374));
#24712=CARTESIAN_POINT('Ctrl Pts',(-23.2871062481768,26.7622670938395,-37.0114839932028));
#24713=CARTESIAN_POINT('Ctrl Pts',(-23.303432721765,26.7635389724028,-37.0104614394955));
#24714=CARTESIAN_POINT('Ctrl Pts',(-23.306916352152,26.763804658643,-37.0102435969431));
#24715=CARTESIAN_POINT('Ctrl Pts',(-23.3124886367667,26.7642205274396,-37.0098957000135));
#24716=CARTESIAN_POINT('Ctrl Pts',(-23.3145770047589,26.7643743391979,-37.0097654408376));
#24717=CARTESIAN_POINT('Ctrl Pts',(-23.3183404813911,26.7646478377678,-37.0095309257412));
#24718=CARTESIAN_POINT('Ctrl Pts',(-23.3200155219303,26.7647682498288,-37.0094266293434));
#24719=CARTESIAN_POINT('Ctrl Pts',(-23.3239938779852,26.7650511125879,-37.0091791087641));
#24720=CARTESIAN_POINT('Ctrl Pts',(-23.3262972721948,26.7652123970623,-37.0090359514058));
#24721=CARTESIAN_POINT('Ctrl Pts',(-23.3321266006297,26.7656142735079,-37.0086740363678));
#24722=CARTESIAN_POINT('Ctrl Pts',(-23.3356527711888,26.7658515420788,-37.0084554662953));
#24723=CARTESIAN_POINT('Ctrl Pts',(-23.3547156750614,26.7671027485429,-37.007275723378));
#24724=CARTESIAN_POINT('Ctrl Pts',(-23.3702595606717,26.7680099080888,-37.0063204866648));
#24725=CARTESIAN_POINT('Ctrl Pts',(-23.6806216219765,26.7838669749509,-36.9873707650317));
#24726=CARTESIAN_POINT('Ctrl Pts',(-23.9761605115232,26.7583558899041,-36.9714544347291));
#24727=CARTESIAN_POINT('Ctrl Pts',(-24.4583366237232,26.64882672026,-36.9436049451794));
#24728=CARTESIAN_POINT('Ctrl Pts',(-24.6480019491708,26.5868142071439,-36.9321405980765));
#24729=CARTESIAN_POINT('Ctrl Pts',(-24.8383934972394,26.5043819107216,-36.9195291295822));
#24730=CARTESIAN_POINT('Ctrl Pts',(-24.8460568316879,26.5010284888284,-36.9190196418501));
#24731=CARTESIAN_POINT('Ctrl Pts',(-24.8582549540482,26.4956339934286,-36.9182056411506));
#24732=CARTESIAN_POINT('Ctrl Pts',(-24.8627982589755,26.4936121776381,-36.9179017877882));
#24733=CARTESIAN_POINT('Ctrl Pts',(-24.8714246283814,26.4897494127858,-36.9173235765552));
#24734=CARTESIAN_POINT('Ctrl Pts',(-24.8755085738406,26.4879104500785,-36.9170492874142));
#24735=CARTESIAN_POINT('Ctrl Pts',(-24.8826343016327,26.4846839177423,-36.9165697387077));
#24736=CARTESIAN_POINT('Ctrl Pts',(-24.8856777900358,26.4833001139089,-36.9163646092205));
#24737=CARTESIAN_POINT('Ctrl Pts',(-24.8915918674088,26.4806000062993,-36.9159654015663));
#24738=CARTESIAN_POINT('Ctrl Pts',(-24.8944626869059,26.4792842136612,-36.915771341228));
#24739=CARTESIAN_POINT('Ctrl Pts',(-24.9012339848637,26.4761686495352,-36.9153129629919));
#24740=CARTESIAN_POINT('Ctrl Pts',(-24.9051328013706,26.47436529799,-36.9150485214087));
#24741=CARTESIAN_POINT('Ctrl Pts',(-24.9186646541965,26.468073425422,-36.9141289130843));
#24742=CARTESIAN_POINT('Ctrl Pts',(-24.9282790055222,26.4635450913197,-36.9134723671469));
#24743=CARTESIAN_POINT('Ctrl Pts',(-25.0443425518691,26.4081763855203,-36.9055078073928));
#24744=CARTESIAN_POINT('Ctrl Pts',(-25.1479324417981,26.3515820047791,-36.897998072312));
#24745=CARTESIAN_POINT('Ctrl Pts',(-25.3288058286702,26.2394651356141,-36.8841218240613));
#24746=CARTESIAN_POINT('Ctrl Pts',(-25.4071822001974,26.1859547482682,-36.8778271556853));
#24747=CARTESIAN_POINT('Ctrl Pts',(-25.5392938429364,26.0869368599996,-36.8667524966644));
#24748=CARTESIAN_POINT('Ctrl Pts',(-25.5941139480393,26.0429785117665,-36.862006474762));
#24749=CARTESIAN_POINT('Ctrl Pts',(-25.7625151588359,25.8986510766886,-36.8469970142875));
#24750=CARTESIAN_POINT('Ctrl Pts',(-25.8704851319537,25.7920391618229,-36.836713848836));
#24751=CARTESIAN_POINT('Ctrl Pts',(-26.0046725470339,25.6394173201056,-36.8233723851675));
#24752=CARTESIAN_POINT('Ctrl Pts',(-26.0378526915846,25.5997971729503,-36.8200220751652));
#24753=CARTESIAN_POINT('Ctrl Pts',(-26.0854536892766,25.5400971853763,-36.8151584874253));
#24754=CARTESIAN_POINT('Ctrl Pts',(-26.1006180932762,25.5206236256763,-36.8136000076198));
#24755=CARTESIAN_POINT('Ctrl Pts',(-26.118150586085,25.4975674760254,-36.8117892564834));
#24756=CARTESIAN_POINT('Ctrl Pts',(-26.1207365479845,25.4941526918522,-36.8115219473492));
#24757=CARTESIAN_POINT('Ctrl Pts',(-26.1246808693452,25.4889225493197,-36.8111138834123));
#24758=CARTESIAN_POINT('Ctrl Pts',(-26.1260441212917,25.4871109131912,-36.8109727839044));
#24759=CARTESIAN_POINT('Ctrl Pts',(-26.1285140162168,25.4838214310551,-36.8107170326233));
#24760=CARTESIAN_POINT('Ctrl Pts',(-26.1296212968025,25.4823440783813,-36.8106023358032));
#24761=CARTESIAN_POINT('Ctrl Pts',(-26.1318647930798,25.4793454013391,-36.8103698622046));
#24762=CARTESIAN_POINT('Ctrl Pts',(-26.1330009293625,25.4778240303005,-36.8102520910679));
#24763=CARTESIAN_POINT('Ctrl Pts',(-26.1362647748683,25.4734454319254,-36.809913635124));
#24764=CARTESIAN_POINT('Ctrl Pts',(-26.1383891005508,25.4705856680496,-36.8096931890154));
#24765=CARTESIAN_POINT('Ctrl Pts',(-26.1476724996088,25.4580449849555,-36.8087291132581));
#24766=CARTESIAN_POINT('Ctrl Pts',(-26.154782150923,25.4483273478671,-36.8079889075632));
#24767=CARTESIAN_POINT('Ctrl Pts',(-26.276580515528,25.27987751124,-36.7952712207404));
#24768=CARTESIAN_POINT('Ctrl Pts',(-26.3766402942151,25.1110292659042,-36.7842407998931));
#24769=CARTESIAN_POINT('Ctrl Pts',(-26.5312661324533,24.7858241499196,-36.7640897792709));
#24770=CARTESIAN_POINT('Ctrl Pts',(-26.5903367750714,24.6323636279976,-36.7549764918937));
#24771=CARTESIAN_POINT('Ctrl Pts',(-26.6778332932944,24.3402872989219,-36.7375080872787));
#24772=CARTESIAN_POINT('Ctrl Pts',(-26.7093362909639,24.2030145175265,-36.7292521282823));
#24773=CARTESIAN_POINT('Ctrl Pts',(-26.7334530381549,24.0537043420488,-36.7200473415056));
#24774=CARTESIAN_POINT('Ctrl Pts',(-26.7350864177421,24.0432660241913,-36.7194027218723));
#24775=CARTESIAN_POINT('Ctrl Pts',(-26.7373626346129,24.028236054932,-36.7184728873856));
#24776=CARTESIAN_POINT('Ctrl Pts',(-26.7380469499211,24.0236506763662,-36.718188989758));
#24777=CARTESIAN_POINT('Ctrl Pts',(-26.7392181017893,24.0156854651227,-36.7176954439549));
#24778=CARTESIAN_POINT('Ctrl Pts',(-26.739709466716,24.012306297254,-36.7174859397762));
#24779=CARTESIAN_POINT('Ctrl Pts',(-26.7406444071193,24.0058040590447,-36.7170825722484));
#24780=CARTESIAN_POINT('Ctrl Pts',(-26.7410887699729,24.0026811041993,-36.7168887341169));
#24781=CARTESIAN_POINT('Ctrl Pts',(-26.7421254813436,23.9953176600328,-36.716431443899));
#24782=CARTESIAN_POINT('Ctrl Pts',(-26.7427139645895,23.9910766398913,-36.7161678695544));
#24783=CARTESIAN_POINT('Ctrl Pts',(-26.7444289284822,23.9785338609437,-36.7153877666544));
#24784=CARTESIAN_POINT('Ctrl Pts',(-26.7455314843335,23.9702289161191,-36.7148704811516));
#24785=CARTESIAN_POINT('Ctrl Pts',(-26.7549960068543,23.8967425880009,-36.7102864490859));
#24786=CARTESIAN_POINT('Ctrl Pts',(-26.7613943232522,23.8313280861149,-36.7061579510891));
#24787=CARTESIAN_POINT('Ctrl Pts',(-26.7671925918538,23.7448164684998,-36.7006289009842));
#24788=CARTESIAN_POINT('Ctrl Pts',(-26.768391966971,23.7238527012756,-36.6992837976909));
#24789=CARTESIAN_POINT('Ctrl Pts',(-26.7718346929764,23.6512402018618,-36.6946063877606));
#24790=CARTESIAN_POINT('Ctrl Pts',(-26.773040024557,23.5995522001169,-36.6912445666056));
#24791=CARTESIAN_POINT('Ctrl Pts',(-26.7728811535608,23.3855807961895,-36.6771997083351));
#24792=CARTESIAN_POINT('Ctrl Pts',(-26.7605037255032,23.2235558296569,-36.6662440056536));
#24793=CARTESIAN_POINT('Ctrl Pts',(-26.710004465697,22.8932709800689,-36.643626532723));
#24794=CARTESIAN_POINT('Ctrl Pts',(-26.6704762752376,22.7257093204273,-36.6319979907716));
#24795=CARTESIAN_POINT('Ctrl Pts',(-26.6057679240138,22.5248380811497,-36.6184114810434));
#24796=CARTESIAN_POINT('Ctrl Pts',(-26.5930900990038,22.4878077135424,-36.6159228844713));
#24797=CARTESIAN_POINT('Ctrl Pts',(-26.578114432191,22.4465349081901,-36.6131744992035));
#24798=CARTESIAN_POINT('Ctrl Pts',(-26.5764787318163,22.4420579335742,-36.6128767115571));
#24799=CARTESIAN_POINT('Ctrl Pts',(-26.5740014261304,22.4353238395941,-36.6124293167212));
#24800=CARTESIAN_POINT('Ctrl Pts',(-26.5731672217961,22.4330640330372,-36.6122792706444));
#24801=CARTESIAN_POINT('Ctrl Pts',(-26.5717184664743,22.429152950119,-36.6120197408775));
#24802=CARTESIAN_POINT('Ctrl Pts',(-26.5711050951413,22.4275012427643,-36.6119101863107));
#24803=CARTESIAN_POINT('Ctrl Pts',(-26.5698246799165,22.4240619418755,-36.6116821667021));
#24804=CARTESIAN_POINT('Ctrl Pts',(-26.5691574037859,22.4222744396219,-36.6115637163916));
#24805=CARTESIAN_POINT('Ctrl Pts',(-26.5675687387622,22.418030224266,-36.6112826054622));
#24806=CARTESIAN_POINT('Ctrl Pts',(-26.5666459336376,22.4155740346287,-36.6111200303186));
#24807=CARTESIAN_POINT('Ctrl Pts',(-26.5635588286077,22.4073876039012,-36.6105785218236));
#24808=CARTESIAN_POINT('Ctrl Pts',(-26.5613811746054,22.4016623613128,-36.6102003879903));
#24809=CARTESIAN_POINT('Ctrl Pts',(-26.5048478548731,22.2542971134466,-36.6004813482129));
#24810=CARTESIAN_POINT('Ctrl Pts',(-26.4405655351955,22.1166421818956,-36.5917321658582));
#24811=CARTESIAN_POINT('Ctrl Pts',(-26.19973517029,21.6835585904831,-36.5637208328264));
#24812=CARTESIAN_POINT('Ctrl Pts',(-25.9856858714323,21.4118035905615,-36.5450819728289));
#24813=CARTESIAN_POINT('Ctrl Pts',(-25.7175259722023,21.1649913424366,-36.5230454433827));
#24814=CARTESIAN_POINT('Ctrl Pts',(-25.7021778644842,21.1511355195344,-36.5217891244063));
#24815=CARTESIAN_POINT('Ctrl Pts',(-25.681989747927,21.133259865776,-36.5201425684659));
#24816=CARTESIAN_POINT('Ctrl Pts',(-25.6772695716875,21.1291049490659,-36.5197580060562));
#24817=CARTESIAN_POINT('Ctrl Pts',(-25.6699868931765,21.122732133314,-36.5191653002192));
#24818=CARTESIAN_POINT('Ctrl Pts',(-25.6674329839928,21.1205044007008,-36.5189575669462));
#24819=CARTESIAN_POINT('Ctrl Pts',(-25.6623772689153,21.1161084075038,-36.5185465696615));
#24820=CARTESIAN_POINT('Ctrl Pts',(-25.6598756261027,21.1139399650641,-36.5183433135708));
#24821=CARTESIAN_POINT('Ctrl Pts',(-25.6543223106103,21.109141276776,-36.5178923562123));
#24822=CARTESIAN_POINT('Ctrl Pts',(-25.6512690418472,21.1065128939125,-36.5176445782382));
#24823=CARTESIAN_POINT('Ctrl Pts',(-25.6425297714073,21.099018245474,-36.5169358306412));
#24824=CARTESIAN_POINT('Ctrl Pts',(-25.6368317641626,21.0941660757891,-36.5164742804625));
#24825=CARTESIAN_POINT('Ctrl Pts',(-25.6003389124298,21.0633090318379,-36.5135217323594));
#24826=CARTESIAN_POINT('Ctrl Pts',(-25.5690765561086,21.037864930152,-36.511007914727));
#24827=CARTESIAN_POINT('Ctrl Pts',(-25.4747252378456,20.9639716121331,-36.5034624939613));
#24828=CARTESIAN_POINT('Ctrl Pts',(-25.4103147885434,20.9172673753464,-36.4983641267141));
#24829=CARTESIAN_POINT('Ctrl Pts',(-25.218329737443,20.7886206919643,-36.4833136717069));
#24830=CARTESIAN_POINT('Ctrl Pts',(-25.0866289468455,20.713241588343,-36.4731572694925));
#24831=CARTESIAN_POINT('Ctrl Pts',(-24.7405448296714,20.5463448226812,-36.4471811271523));
#24832=CARTESIAN_POINT('Ctrl Pts',(-24.5206131289831,20.4682597647843,-36.4312873780352));
#24833=CARTESIAN_POINT('Ctrl Pts',(-24.2812336024695,20.4114691590066,-36.415757384098));
#24834=CARTESIAN_POINT('Ctrl Pts',(-24.2682760643001,20.4084796869861,-36.4149222209012));
#24835=CARTESIAN_POINT('Ctrl Pts',(-24.2517311926241,20.404770274817,-36.413863131888));
#24836=CARTESIAN_POINT('Ctrl Pts',(-24.248160876087,20.4039761796849,-36.4136350167718));
#24837=CARTESIAN_POINT('Ctrl Pts',(-24.2424877415917,20.4027245162911,-36.4132732426204));
#24838=CARTESIAN_POINT('Ctrl Pts',(-24.2403858175467,20.4022629762171,-36.4131393548287));
#24839=CARTESIAN_POINT('Ctrl Pts',(-24.2364960206088,20.4014129384777,-36.4128918654882));
#24840=CARTESIAN_POINT('Ctrl Pts',(-24.2347082908126,20.4010238604602,-36.4127782310411));
#24841=CARTESIAN_POINT('Ctrl Pts',(-24.2307179688395,20.4001589729111,-36.4125248374552));
#24842=CARTESIAN_POINT('Ctrl Pts',(-24.2285152134083,20.3996839520717,-36.4123851245607));
#24843=CARTESIAN_POINT('Ctrl Pts',(-24.2239253542042,20.3986991926628,-36.4120943497092));
#24844=CARTESIAN_POINT('Ctrl Pts',(-24.2215381645779,20.3981898546958,-36.4119433108896));
#24845=CARTESIAN_POINT('Ctrl Pts',(-24.2153568129213,20.3968783235349,-36.4115527085137));
#24846=CARTESIAN_POINT('Ctrl Pts',(-24.2115617635832,20.396080262813,-36.4113133803604));
#24847=CARTESIAN_POINT('Ctrl Pts',(-24.2004375837291,20.393761919072,-36.4106132426767));
#24848=CARTESIAN_POINT('Ctrl Pts',(-24.1931045254415,20.3922603046339,-36.4101534776245));
#24849=CARTESIAN_POINT('Ctrl Pts',(-24.1155988486123,20.3766703655162,-36.4053120563063));
#24850=CARTESIAN_POINT('Ctrl Pts',(-24.0449745415904,20.3648966421247,-36.4010560734304));
#24851=CARTESIAN_POINT('Ctrl Pts',(-23.8948817735102,20.3449881405634,-36.3922274650721));
#24852=CARTESIAN_POINT('Ctrl Pts',(-23.8153855835391,20.3374352335586,-36.3876777045289));
#24853=CARTESIAN_POINT('Ctrl Pts',(-23.6049510279843,20.3253069033151,-36.3757839736858));
#24854=CARTESIAN_POINT('Ctrl Pts',(-23.4738759926402,20.3257473208416,-36.3685241584834));
#24855=CARTESIAN_POINT('Ctrl Pts',(-23.1280552780243,20.3480124141352,-36.3490714349759));
#24856=CARTESIAN_POINT('Ctrl Pts',(-22.9148893781597,20.3834110551393,-36.3367367952457));
#24857=CARTESIAN_POINT('Ctrl Pts',(-22.6941767811211,20.44325642323,-36.3228456656794));
#24858=CARTESIAN_POINT('Ctrl Pts',(-22.6815055205312,20.4467755894092,-36.3220443369211));
#24859=CARTESIAN_POINT('Ctrl Pts',(-22.6643319584784,20.4516585884706,-36.320952962587));
#24860=CARTESIAN_POINT('Ctrl Pts',(-22.6598104583247,20.452954903015,-36.3206651205604));
#24861=CARTESIAN_POINT('Ctrl Pts',(-22.6521529254497,20.4551684721242,-36.3201767789445));
#24862=CARTESIAN_POINT('Ctrl Pts',(-22.6490154101578,20.456080608677,-36.3199764467883));
#24863=CARTESIAN_POINT('Ctrl Pts',(-22.6429754669886,20.4578465034749,-36.3195903200391));
#24864=CARTESIAN_POINT('Ctrl Pts',(-22.640072842781,20.4586995806194,-36.3194045479381));
#24865=CARTESIAN_POINT('Ctrl Pts',(-22.6332275488409,20.4607218788149,-36.3189659401813));
#24866=CARTESIAN_POINT('Ctrl Pts',(-22.6292859142401,20.4618945596411,-36.3187129914275));
#24867=CARTESIAN_POINT('Ctrl Pts',(-22.6178007378814,20.4653354720753,-36.3179747997104));
#24868=CARTESIAN_POINT('Ctrl Pts',(-22.6102632945252,20.4676238085501,-36.3174888979873));
#24869=CARTESIAN_POINT('Ctrl Pts',(-22.5561859923934,20.48425823154,-36.3139923162312));
#24870=CARTESIAN_POINT('Ctrl Pts',(-22.5099703623347,20.4996293295247,-36.3109480518948));
#24871=CARTESIAN_POINT('Ctrl Pts',(-22.3627238818848,20.5523378481134,-36.3010604485225));
#24872=CARTESIAN_POINT('Ctrl Pts',(-22.263218618272,20.5936909739957,-36.2940866565933));
#24873=CARTESIAN_POINT('Ctrl Pts',(-22.0124998480304,20.7129441289156,-36.2757662955648));
#24874=CARTESIAN_POINT('Ctrl Pts',(-21.865046638002,20.79796707663,-36.2642393396158));
#24875=CARTESIAN_POINT('Ctrl Pts',(-21.5771313945329,20.9958249234009,-36.2406128838094));
#24876=CARTESIAN_POINT('Ctrl Pts',(-21.4379889557836,21.1096241579081,-36.2285601998589));
#24877=CARTESIAN_POINT('Ctrl Pts',(-21.3009066345182,21.2422905762718,-36.2165404980373));
#24878=CARTESIAN_POINT('Ctrl Pts',(-21.2928246975247,21.2501949377664,-36.2158313324793));
#24879=CARTESIAN_POINT('Ctrl Pts',(-21.2823124365462,21.2605850084326,-36.2149084326304));
#24880=CARTESIAN_POINT('Ctrl Pts',(-21.2798444355367,21.263032227606,-36.2146917252203));
#24881=CARTESIAN_POINT('Ctrl Pts',(-21.2760466545972,21.2668102332616,-36.2143582071955));
#24882=CARTESIAN_POINT('Ctrl Pts',(-21.2747140827435,21.2681381898866,-36.2142411729082));
#24883=CARTESIAN_POINT('Ctrl Pts',(-21.2720885595176,21.2707592059578,-36.2140105678852));
#24884=CARTESIAN_POINT('Ctrl Pts',(-21.2707955532921,21.2720521915476,-36.2138969930042));
#24885=CARTESIAN_POINT('Ctrl Pts',(-21.2679203003728,21.2749322969241,-36.2136444195745));
#24886=CARTESIAN_POINT('Ctrl Pts',(-21.2663386120602,21.276519963282,-36.2135054659078));
#24887=CARTESIAN_POINT('Ctrl Pts',(-21.2630509578281,21.2798269351842,-36.2132166122395));
#24888=CARTESIAN_POINT('Ctrl Pts',(-21.2613452705144,21.2815465175545,-36.2130667344238));
#24889=CARTESIAN_POINT('Ctrl Pts',(-21.2569452490941,21.2859923959956,-36.2126800604422));
#24890=CARTESIAN_POINT('Ctrl Pts',(-21.2542538276504,21.2887215887428,-36.2124434931255));
#24891=CARTESIAN_POINT('Ctrl Pts',(-21.2464046053484,21.2967094212702,-36.2117534158122));
#24892=CARTESIAN_POINT('Ctrl Pts',(-21.2412599140774,21.3019809928191,-36.2113009144788));
#24893=CARTESIAN_POINT('Ctrl Pts',(-21.1876611514674,21.3572796580724,-36.2065839626036));
#24894=CARTESIAN_POINT('Ctrl Pts',(-21.1408186402256,21.4088515801244,-36.2024385803005));
#24895=CARTESIAN_POINT('Ctrl Pts',(-21.0488727828079,21.5169216021941,-36.1941548209046));
#24896=CARTESIAN_POINT('Ctrl Pts',(-21.0039254065023,21.5734989868452,-36.1900246960718));
#24897=CARTESIAN_POINT('Ctrl Pts',(-20.7543536877596,21.9103008554172,-36.1663062696027));
#24898=CARTESIAN_POINT('Ctrl Pts',(-20.5941768677858,22.2205512124119,-36.1475232007051));
#24899=CARTESIAN_POINT('Ctrl Pts',(-20.480085290229,22.5701388501849,-36.125289718227));
#24900=CARTESIAN_POINT('Ctrl Pts',(-20.4738270685922,22.589962961953,-36.1240266902884));
#24901=CARTESIAN_POINT('Ctrl Pts',(-20.465922369438,22.615873206881,-36.1223725560634));
#24902=CARTESIAN_POINT('Ctrl Pts',(-20.4641012442419,22.621905881726,-36.1219871894567));
#24903=CARTESIAN_POINT('Ctrl Pts',(-20.4613271866338,22.6311936225473,-36.1213935152513));
#24904=CARTESIAN_POINT('Ctrl Pts',(-20.4603616726461,22.6344449400733,-36.1211856199719));
#24905=CARTESIAN_POINT('Ctrl Pts',(-20.4584638951982,22.6408727710267,-36.1207744709013));
#24906=CARTESIAN_POINT('Ctrl Pts',(-20.4575313900382,22.6440492091991,-36.1205712253105));
#24907=CARTESIAN_POINT('Ctrl Pts',(-20.455476058479,22.6510905099913,-36.120120531337));
#24908=CARTESIAN_POINT('Ctrl Pts',(-20.4543555756043,22.6549560458985,-36.1198730067142));
#24909=CARTESIAN_POINT('Ctrl Pts',(-20.4511774820414,22.6659974070521,-36.1191656892814));
#24910=CARTESIAN_POINT('Ctrl Pts',(-20.4491375690422,22.6731782613215,-36.1187053195935));
#24911=CARTESIAN_POINT('Ctrl Pts',(-20.4363405771439,22.7188287350196,-36.115776281397));
#24912=CARTESIAN_POINT('Ctrl Pts',(-20.4262749658969,22.7574870385782,-36.1132852095718));
#24913=CARTESIAN_POINT('Ctrl Pts',(-20.3985070496801,22.8728898581411,-36.1058133343364));
#24914=CARTESIAN_POINT('Ctrl Pts',(-20.3828975020265,22.9501023987676,-36.1007671010837));
#24915=CARTESIAN_POINT('Ctrl Pts',(-20.3456661051738,23.176728242369,-36.0858170493578));
#24916=CARTESIAN_POINT('Ctrl Pts',(-20.3316936141314,23.3271725279076,-36.0757090336739));
#24917=CARTESIAN_POINT('Ctrl Pts',(-20.3238595866909,23.6766461001868,-36.0520800270863));
#24918=CARTESIAN_POINT('Ctrl Pts',(-20.3377822527856,23.8752634143697,-36.0385308482383));
#24919=CARTESIAN_POINT('Ctrl Pts',(-20.377356291198,24.1167929639755,-36.0227036340477));
#24920=CARTESIAN_POINT('Ctrl Pts',(-20.3857768522575,24.1620799896511,-36.0197662173081));
#24921=CARTESIAN_POINT('Ctrl Pts',(-20.3961827088941,24.2120576402219,-36.0165696893483));
#24922=CARTESIAN_POINT('Ctrl Pts',(-20.3972109282809,24.2169391872608,-36.0162579500095));
#24923=CARTESIAN_POINT('Ctrl Pts',(-20.3987641224817,24.224229122287,-36.0157931473617));
#24924=CARTESIAN_POINT('Ctrl Pts',(-20.3992805261228,24.2266392984727,-36.0156395963978));
#24925=CARTESIAN_POINT('Ctrl Pts',(-20.4001738928163,24.2307856224774,-36.0153756469721));
#24926=CARTESIAN_POINT('Ctrl Pts',(-20.4005495262702,24.2325220505968,-36.0152651718622));
#24927=CARTESIAN_POINT('Ctrl Pts',(-20.4013213784783,24.2360758431869,-36.01503920373));
#24928=CARTESIAN_POINT('Ctrl Pts',(-20.4017177340066,24.237893171887,-36.0149237193506));
#24929=CARTESIAN_POINT('Ctrl Pts',(-20.4026336844178,24.2420754988927,-36.0146581089266));
#24930=CARTESIAN_POINT('Ctrl Pts',(-20.4031543730134,24.2444402623517,-36.0145080462252));
#24931=CARTESIAN_POINT('Ctrl Pts',(-20.40426861698,24.2494737019514,-36.01418888265));
#24932=CARTESIAN_POINT('Ctrl Pts',(-20.4048629044418,24.2521422163872,-36.0140198239693));
#24933=CARTESIAN_POINT('Ctrl Pts',(-20.4064623333718,24.2592812668691,-36.0135679317684));
#24934=CARTESIAN_POINT('Ctrl Pts',(-20.4074736193994,24.2637504415804,-36.0132854473559));
#24935=CARTESIAN_POINT('Ctrl Pts',(-20.4105895559033,24.2773855344817,-36.0124248146525));
#24936=CARTESIAN_POINT('Ctrl Pts',(-20.4127248210161,24.286544508467,-36.0118483729121));
#24937=CARTESIAN_POINT('Ctrl Pts',(-20.4206701283094,24.3199627371146,-36.0097507603115));
#24938=CARTESIAN_POINT('Ctrl Pts',(-20.4267218518816,24.344164363953,-36.0082425398103));
#24939=CARTESIAN_POINT('Ctrl Pts',(-20.4594867013519,24.4690168634999,-36.0005067682971));
#24940=CARTESIAN_POINT('Ctrl Pts',(-20.4907881235879,24.5684091604007,-35.9944992791286));
#24941=CARTESIAN_POINT('Ctrl Pts',(-20.650077498447,24.9999980464501,-35.9683945667708));
#24942=CARTESIAN_POINT('Ctrl Pts',(-20.8277370423855,25.3111303006099,-35.9492060091754));
#24943=CARTESIAN_POINT('Ctrl Pts',(-21.0658790383776,25.6031635684743,-35.9264248461005));
#24944=CARTESIAN_POINT('Ctrl Pts',(-21.0792598747683,25.6192500272361,-35.925153634662));
#24945=CARTESIAN_POINT('Ctrl Pts',(-21.0968833364993,25.6400221522051,-35.9234902607903));
#24946=CARTESIAN_POINT('Ctrl Pts',(-21.100984638481,25.644827491231,-35.9231039179832));
#24947=CARTESIAN_POINT('Ctrl Pts',(-21.1075572341329,25.6524826509628,-35.9224859665967));
#24948=CARTESIAN_POINT('Ctrl Pts',(-21.110019462058,25.6553402630607,-35.9222547336004));
#24949=CARTESIAN_POINT('Ctrl Pts',(-21.1144616208505,25.660477476546,-35.9218380326047));
#24950=CARTESIAN_POINT('Ctrl Pts',(-21.1164397520709,25.6627586341387,-35.9216526395398));
#24951=CARTESIAN_POINT('Ctrl Pts',(-21.121083602554,25.6680986873764,-35.9212178015333));
#24952=CARTESIAN_POINT('Ctrl Pts',(-21.1237518942601,25.6711553304408,-35.9209682495042));
#24953=CARTESIAN_POINT('Ctrl Pts',(-21.1314466149519,25.6799364364569,-35.9202494556394));
#24954=CARTESIAN_POINT('Ctrl Pts',(-21.1364875530162,25.6856480976688,-35.9197796071069));
#24955=CARTESIAN_POINT('Ctrl Pts',(-21.1700857386549,25.7234457183815,-35.9166548617271));
#24956=CARTESIAN_POINT('Ctrl Pts',(-21.1992606143772,25.7549745790322,-35.9139739724777));
#24957=CARTESIAN_POINT('Ctrl Pts',(-21.2859458969972,25.8449765666889,-35.9060960928963));
#24958=CARTESIAN_POINT('Ctrl Pts',(-21.3450653380683,25.9018457059962,-35.9008300521178));
#24959=CARTESIAN_POINT('Ctrl Pts',(-21.5332913752687,26.0695625167543,-35.8843785522713));
#24960=CARTESIAN_POINT('Ctrl Pts',(-21.6690463963951,26.1724858591445,-35.8729222430422));
#24961=CARTESIAN_POINT('Ctrl Pts',(-21.8974531629939,26.3187544587974,-35.8545633502822));
#24962=CARTESIAN_POINT('Ctrl Pts',(-21.9851387481169,26.3692523867793,-35.8477131871593));
#24963=CARTESIAN_POINT('Ctrl Pts',(-22.0750360716487,26.4155368035442,-35.8409625058884));
#24964=CARTESIAN_POINT('Origin',(-23.5502525316942,23.5502525316942,-77.3107734492734));
#24965=CARTESIAN_POINT('',(-22.0750360068226,26.4155367701679,-34.3432429022327));
#24966=CARTESIAN_POINT('',(-22.0750360449252,26.4155367897853,-34.591474087242));
#24967=CARTESIAN_POINT('',(-22.0750360153461,26.4155367745563,-77.3107734492734));
#24968=CARTESIAN_POINT('Ctrl Pts',(-22.0750360068226,26.4155367701679,-34.3432429022327));
#24969=CARTESIAN_POINT('Ctrl Pts',(-22.0007070613304,26.3772678657451,-34.3484601301553));
#24970=CARTESIAN_POINT('Ctrl Pts',(-21.9278958678129,26.3361214753991,-34.3537789974476));
#24971=CARTESIAN_POINT('Ctrl Pts',(-21.6840503105524,26.1855166433196,-34.3723350494374));
#24972=CARTESIAN_POINT('Ctrl Pts',(-21.5218199711374,26.0627749939037,-34.3860246494312));
#24973=CARTESIAN_POINT('Ctrl Pts',(-21.3480496407231,25.9034410773503,-34.4019830935093));
#24974=CARTESIAN_POINT('Ctrl Pts',(-21.32420829208,25.8809007179502,-34.4042031017999));
#24975=CARTESIAN_POINT('Ctrl Pts',(-21.2730049423748,25.8309889135581,-34.4090328186539));
#24976=CARTESIAN_POINT('Ctrl Pts',(-21.2457830416468,25.8034803249169,-34.4116405938142));
#24977=CARTESIAN_POINT('Ctrl Pts',(-21.1576217685169,25.7111212547255,-34.4202052703184));
#24978=CARTESIAN_POINT('Ctrl Pts',(-21.0988680152868,25.6442324726953,-34.4261083234741));
#24979=CARTESIAN_POINT('Ctrl Pts',(-21.0135340926948,25.538560847403,-34.4348911343555));
#24980=CARTESIAN_POINT('Ctrl Pts',(-20.9849094514715,25.5014895385991,-34.4378769243289));
#24981=CARTESIAN_POINT('Ctrl Pts',(-20.9541522088457,25.4598088526623,-34.4411181652541));
#24982=CARTESIAN_POINT('Ctrl Pts',(-20.9512124616709,25.4558057176336,-34.4414283047594));
#24983=CARTESIAN_POINT('Ctrl Pts',(-20.9468613481896,25.4498518854977,-34.4418878353512));
#24984=CARTESIAN_POINT('Ctrl Pts',(-20.9454429126368,25.447906401049,-34.4420377178228));
#24985=CARTESIAN_POINT('Ctrl Pts',(-20.9430263346966,25.4445840792636,-34.4422932028219));
#24986=CARTESIAN_POINT('Ctrl Pts',(-20.9420271019281,25.4432080414735,-34.4423988819344));
#24987=CARTESIAN_POINT('Ctrl Pts',(-20.9399776514924,25.4403810512575,-34.4426157105413));
#24988=CARTESIAN_POINT('Ctrl Pts',(-20.9389275565582,25.4389300173834,-34.4427268514098));
#24989=CARTESIAN_POINT('Ctrl Pts',(-20.9364033023714,25.4354358427831,-34.4429941200044));
#24990=CARTESIAN_POINT('Ctrl Pts',(-20.9349303254307,25.4333918434727,-34.4431501650312));
#24991=CARTESIAN_POINT('Ctrl Pts',(-20.9304189952879,25.4271161236867,-34.4436283597811));
#24992=CARTESIAN_POINT('Ctrl Pts',(-20.9273884853667,25.4228787348662,-34.4439499679695));
#24993=CARTESIAN_POINT('Ctrl Pts',(-20.8929677935398,25.3745027707147,-34.4476073694678));
#24994=CARTESIAN_POINT('Ctrl Pts',(-20.862682553646,25.3295837488004,-34.45086875531));
#24995=CARTESIAN_POINT('Ctrl Pts',(-20.8317322380585,25.2810836304513,-34.4542738180806));
#24996=CARTESIAN_POINT('Ctrl Pts',(-20.8299269940291,25.2782449647298,-34.4544726975441));
#24997=CARTESIAN_POINT('Ctrl Pts',(-20.8237610995519,25.268515761665,-34.455152931108));
#24998=CARTESIAN_POINT('Ctrl Pts',(-20.8194221267253,25.2616114533222,-34.4556332520465));
#24999=CARTESIAN_POINT('Ctrl Pts',(-20.6471027308161,24.985087359384,-34.47477775252));
#25000=CARTESIAN_POINT('Ctrl Pts',(-20.519865127747,24.692106104075,-34.49171133187));
#25001=CARTESIAN_POINT('Ctrl Pts',(-20.4078696954906,24.2745906162874,-34.5166057051041));
#25002=CARTESIAN_POINT('Ctrl Pts',(-20.3841170084978,24.1624755286081,-34.5233394322785));
#25003=CARTESIAN_POINT('Ctrl Pts',(-20.3643995472534,24.0366909339388,-34.531045497961));
#25004=CARTESIAN_POINT('Ctrl Pts',(-20.3624917911599,24.0240278069181,-34.531822924568));
#25005=CARTESIAN_POINT('Ctrl Pts',(-20.3596950511249,24.0046818124729,-34.5330132473564));
#25006=CARTESIAN_POINT('Ctrl Pts',(-20.3587514647754,23.9980068692688,-34.5334244183703));
#25007=CARTESIAN_POINT('Ctrl Pts',(-20.3572411559676,23.9870755560331,-34.5340985722942));
#25008=CARTESIAN_POINT('Ctrl Pts',(-20.356661981368,23.982820903975,-34.534361161105));
#25009=CARTESIAN_POINT('Ctrl Pts',(-20.3555611067497,23.9746110799345,-34.5348682399654));
#25010=CARTESIAN_POINT('Ctrl Pts',(-20.3550382441824,23.9706560696495,-34.5351126927685));
#25011=CARTESIAN_POINT('Ctrl Pts',(-20.3540990298016,23.9634487390712,-34.5355584833958));
#25012=CARTESIAN_POINT('Ctrl Pts',(-20.3536802944851,23.960196729889,-34.5357597455015));
#25013=CARTESIAN_POINT('Ctrl Pts',(-20.3528437746979,23.95362088154,-34.5361669550568));
#25014=CARTESIAN_POINT('Ctrl Pts',(-20.3524262086116,23.9502970195201,-34.536372909126));
#25015=CARTESIAN_POINT('Ctrl Pts',(-20.3512634741268,23.9409233995366,-34.5369540723475));
#25016=CARTESIAN_POINT('Ctrl Pts',(-20.3505302887072,23.9348721936124,-34.5373296600194));
#25017=CARTESIAN_POINT('Ctrl Pts',(-20.3475695185783,23.909841549475,-34.5388850052883));
#25018=CARTESIAN_POINT('Ctrl Pts',(-20.345493636209,23.8908448696746,-34.5400695456273));
#25019=CARTESIAN_POINT('Ctrl Pts',(-20.3043252140318,23.4803282855601,-34.5657602552088));
#25020=CARTESIAN_POINT('Ctrl Pts',(-20.3371107642028,23.0849936398098,-34.5929304633547));
#25021=CARTESIAN_POINT('Ctrl Pts',(-20.447889439639,22.6771401084044,-34.6210306599174));
#25022=CARTESIAN_POINT('Ctrl Pts',(-20.455984439751,22.6488718552089,-34.6229754463904));
#25023=CARTESIAN_POINT('Ctrl Pts',(-20.4796015916718,22.5704697376549,-34.6283546355779));
#25024=CARTESIAN_POINT('Ctrl Pts',(-20.4959638763564,22.5205957816201,-34.6317596995402));
#25025=CARTESIAN_POINT('Ctrl Pts',(-20.5220038048327,22.4473171555432,-34.6367155914255));
#25026=CARTESIAN_POINT('Ctrl Pts',(-20.530750016865,22.4235931085398,-34.6383126122323));
#25027=CARTESIAN_POINT('Ctrl Pts',(-20.5413136857066,22.3959461722155,-34.6401629004444));
#25028=CARTESIAN_POINT('Ctrl Pts',(-20.5428606115146,22.3919218408371,-34.6404319615473));
#25029=CARTESIAN_POINT('Ctrl Pts',(-20.5452354656427,22.3857804786619,-34.6408421386363));
#25030=CARTESIAN_POINT('Ctrl Pts',(-20.5460575580257,22.3836612194446,-34.6409836048683));
#25031=CARTESIAN_POINT('Ctrl Pts',(-20.5475514847994,22.3798221003069,-34.6412397334357));
#25032=CARTESIAN_POINT('Ctrl Pts',(-20.548222552607,22.3781019541438,-34.6413544415352));
#25033=CARTESIAN_POINT('Ctrl Pts',(-20.5496896773327,22.3743508018939,-34.6416044734099));
#25034=CARTESIAN_POINT('Ctrl Pts',(-20.5504863160596,22.3723200324708,-34.6417397610191));
#25035=CARTESIAN_POINT('Ctrl Pts',(-20.5526705971863,22.3667685100034,-34.642109402514));
#25036=CARTESIAN_POINT('Ctrl Pts',(-20.5540623856115,22.3632493756113,-34.6423435054442));
#25037=CARTESIAN_POINT('Ctrl Pts',(-20.5608395694614,22.3462011449741,-34.6434766003094));
#25038=CARTESIAN_POINT('Ctrl Pts',(-20.5663105294902,22.3327059219045,-34.6443704842288));
#25039=CARTESIAN_POINT('Ctrl Pts',(-20.5752425792796,22.311095088351,-34.6457977035683));
#25040=CARTESIAN_POINT('Ctrl Pts',(-20.5786457694912,22.3029559987285,-34.6463342572363));
#25041=CARTESIAN_POINT('Ctrl Pts',(-20.5841268726297,22.2899971281019,-34.6471871585642));
#25042=CARTESIAN_POINT('Ctrl Pts',(-20.5861831842435,22.2851683400622,-34.6475046618648));
#25043=CARTESIAN_POINT('Ctrl Pts',(-20.5900432745282,22.2761648591229,-34.6480961230076));
#25044=CARTESIAN_POINT('Ctrl Pts',(-20.5918441079075,22.2719889273544,-34.6483702340477));
#25045=CARTESIAN_POINT('Ctrl Pts',(-20.7187095768812,21.9795062117621,-34.6675547678833));
#25046=CARTESIAN_POINT('Ctrl Pts',(-20.885281299253,21.7109931078188,-34.6843320588523));
#25047=CARTESIAN_POINT('Ctrl Pts',(-21.1846121611122,21.3565741653778,-34.7107036559407));
#25048=CARTESIAN_POINT('Ctrl Pts',(-21.288921514363,21.2491978969512,-34.7193927242447));
#25049=CARTESIAN_POINT('Ctrl Pts',(-21.4114337467225,21.1394860133782,-34.7293273802282));
#25050=CARTESIAN_POINT('Ctrl Pts',(-21.4226382767905,21.1295917600281,-34.7302335402359));
#25051=CARTESIAN_POINT('Ctrl Pts',(-21.4396042541796,21.1148186076509,-34.7316022234323));
#25052=CARTESIAN_POINT('Ctrl Pts',(-21.4453147804074,21.1098813280773,-34.7320623261927));
#25053=CARTESIAN_POINT('Ctrl Pts',(-21.4545581187579,21.1019461869807,-34.7328061663514));
#25054=CARTESIAN_POINT('Ctrl Pts',(-21.4580801640693,21.0989357806865,-34.7330893856879));
#25055=CARTESIAN_POINT('Ctrl Pts',(-21.4648362951719,21.0931862637637,-34.7336322726783));
#25056=CARTESIAN_POINT('Ctrl Pts',(-21.4680693185103,21.090445915105,-34.7338918886557));
#25057=CARTESIAN_POINT('Ctrl Pts',(-21.473832642943,21.0855803573383,-34.7343543887707));
#25058=CARTESIAN_POINT('Ctrl Pts',(-21.4763608294608,21.0834526434339,-34.734557169713));
#25059=CARTESIAN_POINT('Ctrl Pts',(-21.4813703605777,21.0792497822283,-34.7349587730184));
#25060=CARTESIAN_POINT('Ctrl Pts',(-21.4838515663761,21.0771744746477,-34.7351575884958));
#25061=CARTESIAN_POINT('Ctrl Pts',(-21.4905751321485,21.0715679936455,-34.7356960776725));
#25062=CARTESIAN_POINT('Ctrl Pts',(-21.4948234321514,21.0680439897889,-34.7360360433035));
#25063=CARTESIAN_POINT('Ctrl Pts',(-21.5106382774997,21.054993869995,-34.7373005899759));
#25064=CARTESIAN_POINT('Ctrl Pts',(-21.5222620254094,21.0455376599134,-34.7382280019356));
#25065=CARTESIAN_POINT('Ctrl Pts',(-21.7236658190774,20.8840116914442,-34.7542641705081));
#25066=CARTESIAN_POINT('Ctrl Pts',(-21.9299506997231,20.7538558993812,-34.7702790478333));
#25067=CARTESIAN_POINT('Ctrl Pts',(-22.3002996017339,20.5750184727055,-34.7980339945754));
#25068=CARTESIAN_POINT('Ctrl Pts',(-22.4572358536001,20.5138537552655,-34.809503254034));
#25069=CARTESIAN_POINT('Ctrl Pts',(-22.6941778985265,20.4422711913237,-34.8258774608988));
#25070=CARTESIAN_POINT('Ctrl Pts',(-22.7709526250061,20.4221371593679,-34.8310411096143));
#25071=CARTESIAN_POINT('Ctrl Pts',(-22.8634935673152,20.4014878722634,-34.8370362593162));
#25072=CARTESIAN_POINT('Ctrl Pts',(-22.8786126342737,20.3982283206955,-34.8380084971034));
#25073=CARTESIAN_POINT('Ctrl Pts',(-22.8973957773432,20.3943201099858,-34.8392068985248));
#25074=CARTESIAN_POINT('Ctrl Pts',(-22.9010379470199,20.393568858047,-34.8394388360333));
#25075=CARTESIAN_POINT('Ctrl Pts',(-22.9067821638133,20.3923943895788,-34.8398039318364));
#25076=CARTESIAN_POINT('Ctrl Pts',(-22.908883332392,20.391966966658,-34.8399373316242));
#25077=CARTESIAN_POINT('Ctrl Pts',(-22.9128150729242,20.3911712514396,-34.8401866724768));
#25078=CARTESIAN_POINT('Ctrl Pts',(-22.9146455259582,20.3908024555917,-34.8403026417883));
#25079=CARTESIAN_POINT('Ctrl Pts',(-22.9187602749238,20.3899771452007,-34.8405630801412));
#25080=CARTESIAN_POINT('Ctrl Pts',(-22.9210447410607,20.3895215173342,-34.840707497394));
#25081=CARTESIAN_POINT('Ctrl Pts',(-22.9268608490722,20.38836807272,-34.84107473288));
#25082=CARTESIAN_POINT('Ctrl Pts',(-22.9303931804206,20.3876736936584,-34.8412973537434));
#25083=CARTESIAN_POINT('Ctrl Pts',(-22.9500060562038,20.3838523529132,-34.842531168888));
#25084=CARTESIAN_POINT('Ctrl Pts',(-22.9661094790974,20.3808420432346,-34.8435357724718));
#25085=CARTESIAN_POINT('Ctrl Pts',(-23.2954234300031,20.321876612571,-34.8639207198055));
#25086=CARTESIAN_POINT('Ctrl Pts',(-23.6152476167728,20.3124748506111,-34.8809142840806));
#25087=CARTESIAN_POINT('Ctrl Pts',(-24.0912524206191,20.3691550261273,-34.9080681707626));
#25088=CARTESIAN_POINT('Ctrl Pts',(-24.2495220094252,20.4001614242365,-34.9173911876216));
#25089=CARTESIAN_POINT('Ctrl Pts',(-24.4197797009324,20.4469830502476,-34.9280526331369));
#25090=CARTESIAN_POINT('Ctrl Pts',(-24.4347307075587,20.4512111773565,-34.9289941738301));
#25091=CARTESIAN_POINT('Ctrl Pts',(-24.4571085370988,20.4577147274604,-34.9304116353184));
#25092=CARTESIAN_POINT('Ctrl Pts',(-24.4645588061848,20.4599091980298,-34.9308849233698));
#25093=CARTESIAN_POINT('Ctrl Pts',(-24.4765279614739,20.4634817741447,-34.9316475150072));
#25094=CARTESIAN_POINT('Ctrl Pts',(-24.4810519081484,20.4648429313501,-34.9319362643678));
#25095=CARTESIAN_POINT('Ctrl Pts',(-24.489687509176,20.4674619171001,-34.9324884387447));
#25096=CARTESIAN_POINT('Ctrl Pts',(-24.4937996742933,20.4687180373627,-34.9327518073116));
#25097=CARTESIAN_POINT('Ctrl Pts',(-24.5010769097955,20.4709569063961,-34.9332186532455));
#25098=CARTESIAN_POINT('Ctrl Pts',(-24.5042430074497,20.471936316942,-34.9334220206767));
#25099=CARTESIAN_POINT('Ctrl Pts',(-24.5104731382611,20.4738740998323,-34.9338227088392));
#25100=CARTESIAN_POINT('Ctrl Pts',(-24.5135372620037,20.4748321705845,-34.9340200194574));
#25101=CARTESIAN_POINT('Ctrl Pts',(-24.5208886265292,20.4771428128864,-34.9344939874453));
#25102=CARTESIAN_POINT('Ctrl Pts',(-24.5251744705691,20.4784997771241,-34.9347707892889));
#25103=CARTESIAN_POINT('Ctrl Pts',(-24.5407169959546,20.4834565848637,-34.9357763531983));
#25104=CARTESIAN_POINT('Ctrl Pts',(-24.5519565872076,20.487109339865,-34.9365068587834));
#25105=CARTESIAN_POINT('Ctrl Pts',(-24.5684619984128,20.4925739919557,-34.9375845858127));
#25106=CARTESIAN_POINT('Ctrl Pts',(-24.5737437111569,20.4943378772204,-34.9379302092753));
#25107=CARTESIAN_POINT('Ctrl Pts',(-24.8212023356703,20.5776928715304,-34.9541588400366));
#25108=CARTESIAN_POINT('Ctrl Pts',(-25.0527674979565,20.6877677715634,-34.9710531016189));
#25109=CARTESIAN_POINT('Ctrl Pts',(-25.3438339885319,20.8712531007473,-34.9943074855896));
#25110=CARTESIAN_POINT('Ctrl Pts',(-25.416826391595,20.9215885100657,-35.0003205387278));
#25111=CARTESIAN_POINT('Ctrl Pts',(-25.5736540245098,21.0395661349323,-35.0135462940109));
#25112=CARTESIAN_POINT('Ctrl Pts',(-25.6563690687709,21.1085366119362,-35.0207325778132));
#25113=CARTESIAN_POINT('Ctrl Pts',(-25.7728937280232,21.2160343936901,-35.0310091404875));
#25114=CARTESIAN_POINT('Ctrl Pts',(-25.8094840205728,21.2514306556499,-35.0342599627752));
#25115=CARTESIAN_POINT('Ctrl Pts',(-25.8487638998067,21.2912730071509,-35.037761145719));
#25116=CARTESIAN_POINT('Ctrl Pts',(-25.8522965001119,21.2948730580924,-35.0380761250755));
#25117=CARTESIAN_POINT('Ctrl Pts',(-25.857513573421,21.3002147723891,-35.0385414311324));
#25118=CARTESIAN_POINT('Ctrl Pts',(-25.8592045354802,21.3019500437548,-35.0386922672959));
#25119=CARTESIAN_POINT('Ctrl Pts',(-25.8620806909837,21.304908231908,-35.0389488571369));
#25120=CARTESIAN_POINT('Ctrl Pts',(-25.8632668721975,21.3061301813426,-35.0390546891388));
#25121=CARTESIAN_POINT('Ctrl Pts',(-25.8656950077818,21.308635505552,-35.0392713478928));
#25122=CARTESIAN_POINT('Ctrl Pts',(-25.8669368613937,21.3099189698054,-35.0393821667457));
#25123=CARTESIAN_POINT('Ctrl Pts',(-25.8699145708484,21.3130015764623,-35.0396479140008));
#25124=CARTESIAN_POINT('Ctrl Pts',(-25.8716494045566,21.3148017110894,-35.0398027617657));
#25125=CARTESIAN_POINT('Ctrl Pts',(-25.8779228914398,21.3213265166366,-35.040362807074));
#25126=CARTESIAN_POINT('Ctrl Pts',(-25.8824492698307,21.3260630477092,-35.040767049165));
#25127=CARTESIAN_POINT('Ctrl Pts',(-25.9552488809461,21.4027092063204,-35.0472719542793));
#25128=CARTESIAN_POINT('Ctrl Pts',(-26.0201901213056,21.4777268717888,-35.0531222631274));
#25129=CARTESIAN_POINT('Ctrl Pts',(-26.261188018089,21.7835706489239,-35.0755737946021));
#25130=CARTESIAN_POINT('Ctrl Pts',(-26.4091955186267,22.0347318964159,-35.091192604325));
#25131=CARTESIAN_POINT('Ctrl Pts',(-26.5524904703607,22.3759205460712,-35.1125630636644));
#25132=CARTESIAN_POINT('Ctrl Pts',(-26.5806507470381,22.4506283064672,-35.1172412866173));
#25133=CARTESIAN_POINT('Ctrl Pts',(-26.6198092890893,22.5674881632556,-35.1246057655479));
#25134=CARTESIAN_POINT('Ctrl Pts',(-26.6327762319027,22.6089492607536,-35.1272272637293));
#25135=CARTESIAN_POINT('Ctrl Pts',(-26.6470337324432,22.6579957608249,-35.1303425716459));
#25136=CARTESIAN_POINT('Ctrl Pts',(-26.6491405704215,22.6653407438188,-35.1308094748594));
#25137=CARTESIAN_POINT('Ctrl Pts',(-26.6523274107163,22.6766018524368,-35.1315259048349));
#25138=CARTESIAN_POINT('Ctrl Pts',(-26.6534261734689,22.6805126779563,-35.1317748193054));
#25139=CARTESIAN_POINT('Ctrl Pts',(-26.6553288187353,22.6873342661966,-35.1322091893514));
#25140=CARTESIAN_POINT('Ctrl Pts',(-26.6561360116098,22.6902441071061,-35.132394536813));
#25141=CARTESIAN_POINT('Ctrl Pts',(-26.6578145979914,22.6963284114237,-35.132782216677));
#25142=CARTESIAN_POINT('Ctrl Pts',(-26.6586852193673,22.6995030825916,-35.1329845739717));
#25143=CARTESIAN_POINT('Ctrl Pts',(-26.6610781248953,22.7082813865251,-35.1335443195804));
#25144=CARTESIAN_POINT('Ctrl Pts',(-26.6625901250463,22.7138877877499,-35.1339020418571));
#25145=CARTESIAN_POINT('Ctrl Pts',(-26.668456001228,22.7358742726036,-35.1353058433818));
#25146=CARTESIAN_POINT('Ctrl Pts',(-26.6726957229336,22.7522842828809,-35.1363556203747));
#25147=CARTESIAN_POINT('Ctrl Pts',(-26.7409505708434,23.0253429737005,-35.1538592873905));
#25148=CARTESIAN_POINT('Ctrl Pts',(-26.7732447749159,23.2888228325633,-35.1713988181561));
#25149=CARTESIAN_POINT('Ctrl Pts',(-26.772793207378,23.7789236503551,-35.204549075384));
#25150=CARTESIAN_POINT('Ctrl Pts',(-26.7488758700027,24.0040026005548,-35.2199369079335));
#25151=CARTESIAN_POINT('Ctrl Pts',(-26.6987903335703,24.2380105592995,-35.2350465306056));
#25152=CARTESIAN_POINT('Ctrl Pts',(-26.6958689391363,24.2512509818375,-35.2358982074512));
#25153=CARTESIAN_POINT('Ctrl Pts',(-26.6920474792217,24.2680656306222,-35.2369753193334));
#25154=CARTESIAN_POINT('Ctrl Pts',(-26.6912247834463,24.2716570308128,-35.2372051169407));
#25155=CARTESIAN_POINT('Ctrl Pts',(-26.6899104170286,24.277349900225,-35.2375689568062));
#25156=CARTESIAN_POINT('Ctrl Pts',(-26.6894227944469,24.2794522860702,-35.237703232253));
#25157=CARTESIAN_POINT('Ctrl Pts',(-26.6885096552618,24.2833713968149,-35.2379533663661));
#25158=CARTESIAN_POINT('Ctrl Pts',(-26.6880846755762,24.2851882301525,-35.2380692550396));
#25159=CARTESIAN_POINT('Ctrl Pts',(-26.6871299196235,24.2892539889667,-35.2383284395581));
#25160=CARTESIAN_POINT('Ctrl Pts',(-26.6865993038172,24.2915027093179,-35.2384716858026));
#25161=CARTESIAN_POINT('Ctrl Pts',(-26.6850306586588,24.2981187013265,-35.2388928273668));
#25162=CARTESIAN_POINT('Ctrl Pts',(-26.6839859169533,24.3024843999823,-35.2391703346865));
#25163=CARTESIAN_POINT('Ctrl Pts',(-26.6759971432169,24.33556187814,-35.2412700459277));
#25164=CARTESIAN_POINT('Ctrl Pts',(-26.6686674798507,24.3641803586769,-35.2430702961006));
#25165=CARTESIAN_POINT('Ctrl Pts',(-26.6424579619655,24.4609581587167,-35.249114825901));
#25166=CARTESIAN_POINT('Ctrl Pts',(-26.6217274525139,24.5285993442453,-35.2532663110832));
#25167=CARTESIAN_POINT('Ctrl Pts',(-26.5457432739953,24.7502104834999,-35.2667887112144));
#25168=CARTESIAN_POINT('Ctrl Pts',(-26.4809982209221,24.9006599313651,-35.2758495961854));
#25169=CARTESIAN_POINT('Ctrl Pts',(-26.3268836477632,25.1948986463688,-35.2944304041234));
#25170=CARTESIAN_POINT('Ctrl Pts',(-26.2370685923919,25.337863538251,-35.3039316651154));
#25171=CARTESIAN_POINT('Ctrl Pts',(-26.1293323375663,25.4827661252396,-35.3145301944914));
#25172=CARTESIAN_POINT('Ctrl Pts',(-26.1221219819609,25.492351643448,-35.3152360457092));
#25173=CARTESIAN_POINT('Ctrl Pts',(-26.0734315999069,25.5563344356934,-35.3199801803744));
#25174=CARTESIAN_POINT('Ctrl Pts',(-26.0302846707244,25.6094360464178,-35.3240770040704));
#25175=CARTESIAN_POINT('Ctrl Pts',(-25.9793159503632,25.6682367448302,-35.3288167679961));
#25176=CARTESIAN_POINT('Ctrl Pts',(-25.9731176227499,25.675324522614,-35.3293915621143));
#25177=CARTESIAN_POINT('Ctrl Pts',(-25.963994148034,25.6856653980409,-35.3302353124002));
#25178=CARTESIAN_POINT('Ctrl Pts',(-25.9610932562936,25.6889399096257,-35.3305032525866));
#25179=CARTESIAN_POINT('Ctrl Pts',(-25.9559364178062,25.6947370981578,-35.3309789698046));
#25180=CARTESIAN_POINT('Ctrl Pts',(-25.9536831433146,25.6972621522331,-35.3311866342528));
#25181=CARTESIAN_POINT('Ctrl Pts',(-25.9489913528764,25.7025032032666,-35.3316186235982));
#25182=CARTESIAN_POINT('Ctrl Pts',(-25.9465521928283,25.7052186148157,-35.331842975524));
#25183=CARTESIAN_POINT('Ctrl Pts',(-25.940243519563,25.7122178331288,-35.3324226534303));
#25184=CARTESIAN_POINT('Ctrl Pts',(-25.9363671123541,25.716495383724,-35.3327782712085));
#25185=CARTESIAN_POINT('Ctrl Pts',(-25.9200847484293,25.7343659687307,-35.3342696459927));
#25186=CARTESIAN_POINT('Ctrl Pts',(-25.9075741612623,25.747862814132,-35.3354098555917));
#25187=CARTESIAN_POINT('Ctrl Pts',(-25.8225516701534,25.8380265464535,-35.3431218734403));
#25188=CARTESIAN_POINT('Ctrl Pts',(-25.7464350338262,25.9111912373882,-35.3498507788165));
#25189=CARTESIAN_POINT('Ctrl Pts',(-25.5522071166439,26.0803548767304,-35.3666304963467));
#25190=CARTESIAN_POINT('Ctrl Pts',(-25.4306267117162,26.1719742093008,-35.3768231084262));
#25191=CARTESIAN_POINT('Ctrl Pts',(-25.1090873148588,26.3803717305367,-35.4027306334987));
#25192=CARTESIAN_POINT('Ctrl Pts',(-24.902148397357,26.4848632156532,-35.4185125111137));
#25193=CARTESIAN_POINT('Ctrl Pts',(-24.6732284693989,26.5710509133089,-35.4339548712004));
#25194=CARTESIAN_POINT('Ctrl Pts',(-24.6606338391312,26.5757031074226,-35.4347981624847));
#25195=CARTESIAN_POINT('Ctrl Pts',(-24.6445590105154,26.5815269117716,-35.4358661222886));
#25196=CARTESIAN_POINT('Ctrl Pts',(-24.6411056236721,26.5827713805962,-35.4360950649816));
#25197=CARTESIAN_POINT('Ctrl Pts',(-24.635621471982,26.584737079355,-35.4364578529398));
#25198=CARTESIAN_POINT('Ctrl Pts',(-24.6335921103004,26.5854621725633,-35.4365919291411));
#25199=CARTESIAN_POINT('Ctrl Pts',(-24.6298386752978,26.5867990351575,-35.4368395949772));
#25200=CARTESIAN_POINT('Ctrl Pts',(-24.6281148194717,26.5874113681351,-35.4369532178803));
#25201=CARTESIAN_POINT('Ctrl Pts',(-24.6242698576531,26.5887734559585,-35.4372063724033));
#25202=CARTESIAN_POINT('Ctrl Pts',(-24.6221484923312,26.5895224560834,-35.4373458581969));
#25203=CARTESIAN_POINT('Ctrl Pts',(-24.6177289696364,26.5910776743824,-35.437636070281));
#25204=CARTESIAN_POINT('Ctrl Pts',(-24.6154306779065,26.5918835104441,-35.4377867736952));
#25205=CARTESIAN_POINT('Ctrl Pts',(-24.60948259095,26.5939614835027,-35.4381762478616));
#25206=CARTESIAN_POINT('Ctrl Pts',(-24.6058314033714,26.5952296658916,-35.4384147850919));
#25207=CARTESIAN_POINT('Ctrl Pts',(-24.5951349559917,26.5989233568611,-35.4391120477866));
#25208=CARTESIAN_POINT('Ctrl Pts',(-24.5880834972502,26.6013310246709,-35.4395697390501));
#25209=CARTESIAN_POINT('Ctrl Pts',(-24.5137318223007,26.6264302621811,-35.4443756338971));
#25210=CARTESIAN_POINT('Ctrl Pts',(-24.445701495991,26.6469176209216,-35.4486000670434));
#25211=CARTESIAN_POINT('Ctrl Pts',(-24.3007011453494,26.6854053665977,-35.4573508684769));
#25212=CARTESIAN_POINT('Ctrl Pts',(-24.2236347675704,26.7028568755086,-35.4618552314217));
#25213=CARTESIAN_POINT('Ctrl Pts',(-23.8120524852248,26.7802751058987,-35.4854956806251));
#25214=CARTESIAN_POINT('Ctrl Pts',(-23.470311643524,26.7898800181453,-35.5039590711322));
#25215=CARTESIAN_POINT('Ctrl Pts',(-23.1137147143978,26.7433615719101,-35.5257141041009));
#25216=CARTESIAN_POINT('Ctrl Pts',(-23.0940803238998,26.7406157552393,-35.5269190354536));
#25217=CARTESIAN_POINT('Ctrl Pts',(-23.0683555791806,26.7367758949315,-35.5285074249098));
#25218=CARTESIAN_POINT('Ctrl Pts',(-23.0622409811886,26.7358451834671,-35.5288856948257));
#25219=CARTESIAN_POINT('Ctrl Pts',(-23.0528009056605,26.7343804791909,-35.5294708158884));
#25220=CARTESIAN_POINT('Ctrl Pts',(-23.0494734991666,26.7338588620555,-35.5296772736403));
#25221=CARTESIAN_POINT('Ctrl Pts',(-23.0428441129958,26.7328089634501,-35.5300890449534));
#25222=CARTESIAN_POINT('Ctrl Pts',(-23.0395421255566,26.7322807568371,-35.5302943558999));
#25223=CARTESIAN_POINT('Ctrl Pts',(-23.0322171070506,26.7310973055674,-35.530750289477));
#25224=CARTESIAN_POINT('Ctrl Pts',(-23.0281944898826,26.7304395666653,-35.5310009911626));
#25225=CARTESIAN_POINT('Ctrl Pts',(-23.0165705046972,26.728516277686,-35.5317263660063));
#25226=CARTESIAN_POINT('Ctrl Pts',(-23.0089724530998,26.7272310994357,-35.5322016633369));
#25227=CARTESIAN_POINT('Ctrl Pts',(-22.9572207793516,26.7182864826373,-35.5354469557434));
#25228=CARTESIAN_POINT('Ctrl Pts',(-22.9132283329123,26.7097343905958,-35.5382452937435));
#25229=CARTESIAN_POINT('Ctrl Pts',(-22.8163890395407,26.6888042241506,-35.544497113407));
#25230=CARTESIAN_POINT('Ctrl Pts',(-22.7636486034597,26.6760030091301,-35.5479632841837));
#25231=CARTESIAN_POINT('Ctrl Pts',(-22.6342331843538,26.641108466781,-35.5566226176568));
#25232=CARTESIAN_POINT('Ctrl Pts',(-22.5580103071176,26.6174883683902,-35.5618589955983));
#25233=CARTESIAN_POINT('Ctrl Pts',(-22.3428831416392,26.54196597949,-35.5770063263489));
#25234=CARTESIAN_POINT('Ctrl Pts',(-22.2066622590385,26.4833057049606,-35.5870567917328));
#25235=CARTESIAN_POINT('Ctrl Pts',(-22.0750357765539,26.4155366516121,-35.5970690335682));
#25236=CARTESIAN_POINT('',(-26.773002305904,23.5490461609309,-35.4331262776897));
#25237=CARTESIAN_POINT('Ctrl Pts',(-22.0750360716487,26.4155368035442,-35.8409625058884));
#25238=CARTESIAN_POINT('Ctrl Pts',(-22.1102710601675,26.4336778430016,-35.8383165964471));
#25239=CARTESIAN_POINT('Ctrl Pts',(-22.1458458370451,26.4511716035792,-35.8356862541541));
#25240=CARTESIAN_POINT('Ctrl Pts',(-22.251482879974,26.5007183571307,-35.8280127797491));
#25241=CARTESIAN_POINT('Ctrl Pts',(-22.3223804309384,26.5309208493099,-35.8230368370741));
#25242=CARTESIAN_POINT('Ctrl Pts',(-22.4000755463446,26.5607755364305,-35.817820286076));
#25243=CARTESIAN_POINT('Ctrl Pts',(-22.4058586657744,26.5629786295714,-35.8174333947282));
#25244=CARTESIAN_POINT('Ctrl Pts',(-22.4139306478428,26.5660270742643,-35.8168953569739));
#25245=CARTESIAN_POINT('Ctrl Pts',(-22.416214130997,26.5668864871443,-35.816743371817));
#25246=CARTESIAN_POINT('Ctrl Pts',(-22.4201558521784,26.5683648871744,-35.8164813996653));
#25247=CARTESIAN_POINT('Ctrl Pts',(-22.4218136237979,26.5689851012564,-35.8163713386144));
#25248=CARTESIAN_POINT('Ctrl Pts',(-22.425218250789,26.5702556614475,-35.8161455429463));
#25249=CARTESIAN_POINT('Ctrl Pts',(-22.426965156706,26.5709058567447,-35.8160298179407));
#25250=CARTESIAN_POINT('Ctrl Pts',(-22.4310705455282,26.5724298213702,-35.8157581574488));
#25251=CARTESIAN_POINT('Ctrl Pts',(-22.4334294954344,26.5733023483818,-35.8156022971143));
#25252=CARTESIAN_POINT('Ctrl Pts',(-22.4384200396872,26.5751416093315,-35.8152730549435));
#25253=CARTESIAN_POINT('Ctrl Pts',(-22.4410518811418,26.5761076735091,-35.8150997132645));
#25254=CARTESIAN_POINT('Ctrl Pts',(-22.4481475888601,26.5787017774224,-35.814633137517));
#25255=CARTESIAN_POINT('Ctrl Pts',(-22.4526138219289,26.580323389359,-35.8143402830806));
#25256=CARTESIAN_POINT('Ctrl Pts',(-22.4663785782171,26.5852867068029,-35.8134401962355));
#25257=CARTESIAN_POINT('Ctrl Pts',(-22.47568900116,26.5885955695641,-35.8128348596844));
#25258=CARTESIAN_POINT('Ctrl Pts',(-22.5101965692175,26.6006808732127,-35.8106036145321));
#25259=CARTESIAN_POINT('Ctrl Pts',(-22.5354879749682,26.6091873903452,-35.8089925511983));
#25260=CARTESIAN_POINT('Ctrl Pts',(-22.6250410973573,26.6380747305811,-35.8033636111943));
#25261=CARTESIAN_POINT('Ctrl Pts',(-22.6898372002171,26.6567535884842,-35.7994269386415));
#25262=CARTESIAN_POINT('Ctrl Pts',(-23.1353794936148,26.770178206605,-35.7729834020887));
#25263=CARTESIAN_POINT('Ctrl Pts',(-23.5300430090044,26.7967389386153,-35.7521744414144));
#25264=CARTESIAN_POINT('Ctrl Pts',(-23.9389670105545,26.7495320474123,-35.7272640303427));
#25265=CARTESIAN_POINT('Ctrl Pts',(-23.9580757106773,26.7471523730092,-35.7260934507402));
#25266=CARTESIAN_POINT('Ctrl Pts',(-23.9832220495494,26.7437916881667,-35.7245440337353));
#25267=CARTESIAN_POINT('Ctrl Pts',(-23.9892801281293,26.7429645005491,-35.7241700715772));
#25268=CARTESIAN_POINT('Ctrl Pts',(-23.9986575567256,26.7416568847585,-35.7235901304561));
#25269=CARTESIAN_POINT('Ctrl Pts',(-24.0019785951039,26.7411885032755,-35.7233845335682));
#25270=CARTESIAN_POINT('Ctrl Pts',(-24.0086109207714,26.7402425539957,-35.7229735226799));
#25271=CARTESIAN_POINT('Ctrl Pts',(-24.0119222076893,26.7397650125216,-35.7227681097491));
#25272=CARTESIAN_POINT('Ctrl Pts',(-24.0192906216346,26.7386906523412,-35.7223105469557));
#25273=CARTESIAN_POINT('Ctrl Pts',(-24.023347360047,26.7380912450151,-35.7220583152393));
#25274=CARTESIAN_POINT('Ctrl Pts',(-24.0351389005028,26.7363259706419,-35.7213242368148));
#25275=CARTESIAN_POINT('Ctrl Pts',(-24.0428705751676,26.7351396899056,-35.7208417425549));
#25276=CARTESIAN_POINT('Ctrl Pts',(-24.097428146185,26.7265654347395,-35.7174287829519));
#25277=CARTESIAN_POINT('Ctrl Pts',(-24.1440882455517,26.7181735485475,-35.7144665292356));
#25278=CARTESIAN_POINT('Ctrl Pts',(-24.2904466673276,26.688503768653,-35.7050312468401));
#25279=CARTESIAN_POINT('Ctrl Pts',(-24.3893221687627,26.6635252045523,-35.6984430715252));
#25280=CARTESIAN_POINT('Ctrl Pts',(-24.6284224582453,26.5909040938203,-35.6819927431484));
#25281=CARTESIAN_POINT('Ctrl Pts',(-24.7668648740075,26.5382050817035,-35.6720093853569));
#25282=CARTESIAN_POINT('Ctrl Pts',(-24.9665288773683,26.4460181806787,-35.6571229153511));
#25283=CARTESIAN_POINT('Ctrl Pts',(-25.0308432890317,26.413668094698,-35.6522499022575));
#25284=CARTESIAN_POINT('Ctrl Pts',(-25.1987209230725,26.3220562659645,-35.6393937959507));
#25285=CARTESIAN_POINT('Ctrl Pts',(-25.3001795653451,26.2591462882303,-35.6314789242579));
#25286=CARTESIAN_POINT('Ctrl Pts',(-25.4002781557176,26.1891028491708,-35.6236839281037));
#25287=CARTESIAN_POINT('Ctrl Pts',(-25.4026286123673,26.1874534462055,-35.6235009004112));
#25288=CARTESIAN_POINT('Ctrl Pts',(-25.4244144518681,26.1721220156394,-35.6218045739079));
#25289=CARTESIAN_POINT('Ctrl Pts',(-25.4437008155392,26.1582280245069,-35.6203037122082));
#25290=CARTESIAN_POINT('Ctrl Pts',(-25.4661264770231,26.1416925442678,-35.618561251092));
#25291=CARTESIAN_POINT('Ctrl Pts',(-25.46941597309,26.1392573595785,-35.6183057280522));
#25292=CARTESIAN_POINT('Ctrl Pts',(-25.4746698179196,26.1353524696976,-35.6178977397995));
#25293=CARTESIAN_POINT('Ctrl Pts',(-25.4766371292445,26.1338867866548,-35.6177449954255));
#25294=CARTESIAN_POINT('Ctrl Pts',(-25.4800846194524,26.1313122164113,-35.6174773793935));
#25295=CARTESIAN_POINT('Ctrl Pts',(-25.4815655184702,26.1302043006607,-35.6173624392838));
#25296=CARTESIAN_POINT('Ctrl Pts',(-25.4846446890758,26.1278965214748,-35.6171234849175));
#25297=CARTESIAN_POINT('Ctrl Pts',(-25.4862427953862,26.126696448323,-35.616999486122));
#25298=CARTESIAN_POINT('Ctrl Pts',(-25.4903536107411,26.1236035108993,-35.6166805716164));
#25299=CARTESIAN_POINT('Ctrl Pts',(-25.4928646739391,26.1217084469489,-35.6164858112233));
#25300=CARTESIAN_POINT('Ctrl Pts',(-25.5031164000837,26.1139480272504,-35.6156908490718));
#25301=CARTESIAN_POINT('Ctrl Pts',(-25.5108334105347,26.1080512934506,-35.6150928392398));
#25302=CARTESIAN_POINT('Ctrl Pts',(-25.5304873217621,26.0928921076946,-35.6135704978678));
#25303=CARTESIAN_POINT('Ctrl Pts',(-25.5423861053713,26.0835803197966,-35.6126495022508));
#25304=CARTESIAN_POINT('Ctrl Pts',(-25.5913610248482,26.0446949261278,-35.6088593843651));
#25305=CARTESIAN_POINT('Ctrl Pts',(-25.6278494990012,26.014386882081,-35.6060371482327));
#25306=CARTESIAN_POINT('Ctrl Pts',(-25.7307068847924,25.9250417818928,-35.5980423371901));
#25307=CARTESIAN_POINT('Ctrl Pts',(-25.7953244459871,25.8640501281224,-35.5929704918099));
#25308=CARTESIAN_POINT('Ctrl Pts',(-26.0948797477136,25.5569227432061,-35.5687497110011));
#25309=CARTESIAN_POINT('Ctrl Pts',(-26.292333685706,25.2773414137618,-35.5502689330145));
#25310=CARTESIAN_POINT('Ctrl Pts',(-26.4512012453136,24.9541794048019,-35.5284858410977));
#25311=CARTESIAN_POINT('Ctrl Pts',(-26.4598205427123,24.9362280241387,-35.5272756019372));
#25312=CARTESIAN_POINT('Ctrl Pts',(-26.4709027943603,24.9125880252599,-35.5256811838719));
#25313=CARTESIAN_POINT('Ctrl Pts',(-26.4735166138941,24.9069702837387,-35.5253022423404));
#25314=CARTESIAN_POINT('Ctrl Pts',(-26.4775271931732,24.8982851642112,-35.5247163051081));
#25315=CARTESIAN_POINT('Ctrl Pts',(-26.4789353788422,24.8952230528402,-35.5245097045662));
#25316=CARTESIAN_POINT('Ctrl Pts',(-26.4817311405975,24.8891184362096,-35.524097790502));
#25317=CARTESIAN_POINT('Ctrl Pts',(-26.4831187899893,24.8860759689611,-35.5238924798248));
#25318=CARTESIAN_POINT('Ctrl Pts',(-26.4861859744864,24.8793232479665,-35.5234367533396));
#25319=CARTESIAN_POINT('Ctrl Pts',(-26.4878632147489,24.8756119636666,-35.523186258876));
#25320=CARTESIAN_POINT('Ctrl Pts',(-26.4926868982587,24.8648843017093,-35.5224621049292));
#25321=CARTESIAN_POINT('Ctrl Pts',(-26.495815254209,24.8578598650942,-35.5219878245647));
#25322=CARTESIAN_POINT('Ctrl Pts',(-26.5168579384732,24.8101517381909,-35.5187658258118));
#25323=CARTESIAN_POINT('Ctrl Pts',(-26.5339532387647,24.7691140584656,-35.5159902273843));
#25324=CARTESIAN_POINT('Ctrl Pts',(-26.5527607584845,24.7211971406555,-35.512742594729));
#25325=CARTESIAN_POINT('Ctrl Pts',(-26.5553064642967,24.7146484223127,-35.5122986046544));
#25326=CARTESIAN_POINT('Ctrl Pts',(-26.5997588381729,24.5991798668501,-35.504467495601));
#25327=CARTESIAN_POINT('Ctrl Pts',(-26.635735585645,24.4880831732943,-35.4968877360105));
#25328=CARTESIAN_POINT('Ctrl Pts',(-26.7370147295979,24.1056518915583,-35.470687784072));
#25329=CARTESIAN_POINT('Ctrl Pts',(-26.7731066982184,23.8279241956221,-35.4513695415814));
#25330=CARTESIAN_POINT('Ctrl Pts',(-26.773002305904,23.5490461609309,-35.4331262776897));
#25331=CARTESIAN_POINT('Ctrl Pts',(-26.7730023043127,23.5490419171598,-35.4331260000766));
#25332=CARTESIAN_POINT('Ctrl Pts',(-26.7729772287911,23.4822889340426,-35.4287592473437));
#25333=CARTESIAN_POINT('Ctrl Pts',(-26.7708781614745,23.4155458727867,-35.4244662071997));
#25334=CARTESIAN_POINT('Ctrl Pts',(-26.7664586286456,23.3449437509865,-35.4200355072642));
#25335=CARTESIAN_POINT('Ctrl Pts',(-26.7662030275764,23.3409781616955,-35.4197870141426));
#25336=CARTESIAN_POINT('Ctrl Pts',(-26.765775929236,23.3345374468629,-35.419384037734));
#25337=CARTESIAN_POINT('Ctrl Pts',(-26.7656089083806,23.3320620439012,-35.4192293064516));
#25338=CARTESIAN_POINT('Ctrl Pts',(-26.7653110094593,23.3277215389382,-35.4189582536014));
#25339=CARTESIAN_POINT('Ctrl Pts',(-26.7651813668746,23.3258563575859,-35.4188418626807));
#25340=CARTESIAN_POINT('Ctrl Pts',(-26.7649255672512,23.3222218686168,-35.4186152298821));
#25341=CARTESIAN_POINT('Ctrl Pts',(-26.7647995723652,23.3204525486392,-35.4185049787189));
#25342=CARTESIAN_POINT('Ctrl Pts',(-26.7645459770347,23.316932383729,-35.4182857816497));
#25343=CARTESIAN_POINT('Ctrl Pts',(-26.7644184069459,23.3151815411187,-35.4181768341698));
#25344=CARTESIAN_POINT('Ctrl Pts',(-26.7641142346499,23.3110534530344,-35.417920137494));
#25345=CARTESIAN_POINT('Ctrl Pts',(-26.7639364250196,23.3086762935752,-35.4177724568808));
#25346=CARTESIAN_POINT('Ctrl Pts',(-26.7634025997687,23.3016444151936,-35.4173360056764));
#25347=CARTESIAN_POINT('Ctrl Pts',(-26.7630391056958,23.296990244488,-35.4170476553558));
#25348=CARTESIAN_POINT('Ctrl Pts',(-26.7597522742334,23.2560518271307,-35.4145157738777));
#25349=CARTESIAN_POINT('Ctrl Pts',(-26.7562243361318,23.2198168870903,-35.4123056700737));
#25350=CARTESIAN_POINT('Ctrl Pts',(-26.7508322708735,23.1727240080317,-35.409464540639));
#25351=CARTESIAN_POINT('Ctrl Pts',(-26.749525617909,23.161806680405,-35.4088080873048));
#25352=CARTESIAN_POINT('Ctrl Pts',(-26.7478631325033,23.1484940620951,-35.4080100514496));
#25353=CARTESIAN_POINT('Ctrl Pts',(-26.7475604569788,23.14609234896,-35.4078661759724));
#25354=CARTESIAN_POINT('Ctrl Pts',(-26.7458586310083,23.1327100165865,-35.4070650330177));
#25355=CARTESIAN_POINT('Ctrl Pts',(-26.7444056038027,23.1217361937076,-35.4064100676666));
#25356=CARTESIAN_POINT('Ctrl Pts',(-26.7412587244769,23.0988755296853,-35.4050493938619));
#25357=CARTESIAN_POINT('Ctrl Pts',(-26.7395549243022,23.0869902128819,-35.4043440936909));
#25358=CARTESIAN_POINT('Ctrl Pts',(-26.6899075509956,22.7539235962406,-35.3846317756214));
#25359=CARTESIAN_POINT('Ctrl Pts',(-26.5937600794297,22.4417934065153,-35.3673435633832));
#25360=CARTESIAN_POINT('Ctrl Pts',(-26.4186385468106,22.0790053562045,-35.3440268468972));
#25361=CARTESIAN_POINT('Ctrl Pts',(-26.382178021969,22.0099917746236,-35.3394427555385));
#25362=CARTESIAN_POINT('Ctrl Pts',(-26.3234807842531,21.9080305979578,-35.3323991552882));
#25363=CARTESIAN_POINT('Ctrl Pts',(-26.3030795179905,21.8740570806548,-35.3300050819726));
#25364=CARTESIAN_POINT('Ctrl Pts',(-26.2781062722816,21.8341560876949,-35.3271335975027));
#25365=CARTESIAN_POINT('Ctrl Pts',(-26.2741329988635,21.8278564581246,-35.3266784491115));
#25366=CARTESIAN_POINT('Ctrl Pts',(-26.2679810834712,21.8181771147889,-35.3259763256984));
#25367=CARTESIAN_POINT('Ctrl Pts',(-26.2658178757311,21.814787581595,-35.3257299252481));
#25368=CARTESIAN_POINT('Ctrl Pts',(-26.2620210750723,21.8088628494251,-35.3252982985042));
#25369=CARTESIAN_POINT('Ctrl Pts',(-26.2603902529755,21.8063258732707,-35.325113175787));
#25370=CARTESIAN_POINT('Ctrl Pts',(-26.2566971850662,21.8005984709031,-35.3246945683901));
#25371=CARTESIAN_POINT('Ctrl Pts',(-26.2546328571561,21.7974093985914,-35.3244610060081));
#25372=CARTESIAN_POINT('Ctrl Pts',(-26.2490551403864,21.7888259834855,-35.3238310774499));
#25373=CARTESIAN_POINT('Ctrl Pts',(-26.2455312326205,21.7834385265459,-35.323434317128));
#25374=CARTESIAN_POINT('Ctrl Pts',(-26.2299135711976,21.7597172304439,-35.3216812232514));
#25375=CARTESIAN_POINT('Ctrl Pts',(-26.2176489510915,21.7414970880346,-35.3203184627856));
#25376=CARTESIAN_POINT('Ctrl Pts',(-26.1979493648319,21.7128678096268,-35.3181509062968));
#25377=CARTESIAN_POINT('Ctrl Pts',(-26.1906368642594,21.7023749097116,-35.3173508118052));
#25378=CARTESIAN_POINT('Ctrl Pts',(-26.1757047245593,21.6812179892695,-35.3157259779533));
#25379=CARTESIAN_POINT('Ctrl Pts',(-26.1680821070627,21.6705563743447,-35.3149011346751));
#25380=CARTESIAN_POINT('Ctrl Pts',(-26.1563518490074,21.6543592278252,-35.3136387239792));
#25381=CARTESIAN_POINT('Ctrl Pts',(-26.1522910672432,21.6487897974573,-35.3132029465036));
#25382=CARTESIAN_POINT('Ctrl Pts',(-26.1447758475971,21.6385517038732,-35.3123987354935));
#25383=CARTESIAN_POINT('Ctrl Pts',(-26.1413265891683,21.6338792591201,-35.3120304997206));
#25384=CARTESIAN_POINT('Ctrl Pts',(-26.1354508134646,21.6259646618885,-35.3114046865719));
#25385=CARTESIAN_POINT('Ctrl Pts',(-26.1330307716773,21.6227177006777,-35.3111473547322));
#25386=CARTESIAN_POINT('Ctrl Pts',(-26.1268553438013,21.6144646623879,-35.3104917648633));
#25387=CARTESIAN_POINT('Ctrl Pts',(-26.1230914966107,21.609464963195,-35.3100931883706));
#25388=CARTESIAN_POINT('Ctrl Pts',(-26.1046789443896,21.5851543763156,-35.3081482062688));
#25389=CARTESIAN_POINT('Ctrl Pts',(-26.0898275629079,21.56599859903,-35.3065942185389));
#25390=CARTESIAN_POINT('Ctrl Pts',(-25.8882963309084,21.3120262959302,-35.28570179583));
#25391=CARTESIAN_POINT('Ctrl Pts',(-25.6699470611983,21.1042472797076,-35.2650663614345));
#25392=CARTESIAN_POINT('Ctrl Pts',(-25.3698430332791,20.8894266154983,-35.2403994929138));
#25393=CARTESIAN_POINT('Ctrl Pts',(-25.3122997712607,20.8509758007019,-35.2358226826034));
#25394=CARTESIAN_POINT('Ctrl Pts',(-25.2229634706317,20.7953560384084,-35.2289930548825));
#25395=CARTESIAN_POINT('Ctrl Pts',(-25.1920480787276,20.7768206858367,-35.2266779127681));
#25396=CARTESIAN_POINT('Ctrl Pts',(-25.1501596179288,20.7526523911278,-35.2236117789459));
#25397=CARTESIAN_POINT('Ctrl Pts',(-25.1394570294634,20.7465588418231,-35.2228344721761));
#25398=CARTESIAN_POINT('Ctrl Pts',(-25.1214967785109,20.7364690089506,-35.2215405593965));
#25399=CARTESIAN_POINT('Ctrl Pts',(-25.1142582661286,20.732439148541,-35.2210219063457));
#25400=CARTESIAN_POINT('Ctrl Pts',(-25.1044169892618,20.727009869037,-35.220320678601));
#25401=CARTESIAN_POINT('Ctrl Pts',(-25.1018278041891,20.7255860969865,-35.2201365560972));
#25402=CARTESIAN_POINT('Ctrl Pts',(-25.0977046983941,20.7233262139067,-35.2198439406262));
#25403=CARTESIAN_POINT('Ctrl Pts',(-25.0961720576621,20.7224877901201,-35.2197352985571));
#25404=CARTESIAN_POINT('Ctrl Pts',(-25.0929827772985,20.7207464773732,-35.2195094939903));
#25405=CARTESIAN_POINT('Ctrl Pts',(-25.0913260306343,20.7198437991928,-35.2193923456736));
#25406=CARTESIAN_POINT('Ctrl Pts',(-25.0875137868304,20.7177710381644,-35.219123128286));
#25407=CARTESIAN_POINT('Ctrl Pts',(-25.0853577407189,20.7166019577784,-35.2189711240067));
#25408=CARTESIAN_POINT('Ctrl Pts',(-25.0786768277215,20.712989205944,-35.2185008893086));
#25409=CARTESIAN_POINT('Ctrl Pts',(-25.0741474163586,20.7105538875253,-35.2181831929319));
#25410=CARTESIAN_POINT('Ctrl Pts',(-25.036998327253,20.6906944994713,-35.2155864094124));
#25411=CARTESIAN_POINT('Ctrl Pts',(-25.0040850920372,20.6738213446743,-35.2133417191707));
#25412=CARTESIAN_POINT('Ctrl Pts',(-24.9636240488202,20.6539507535484,-35.2106410446163));
#25413=CARTESIAN_POINT('Ctrl Pts',(-24.9563476162302,20.6504112168324,-35.210157649367));
#25414=CARTESIAN_POINT('Ctrl Pts',(-24.8096683027272,20.5797426575786,-35.2004577434593));
#25415=CARTESIAN_POINT('Ctrl Pts',(-24.6656073222198,20.522703824847,-35.1917311718961));
#25416=CARTESIAN_POINT('Ctrl Pts',(-24.5025675691141,20.4713769063217,-35.1821603804128));
#25417=CARTESIAN_POINT('Ctrl Pts',(-24.4871069909883,20.4666373203632,-35.1812558327212));
#25418=CARTESIAN_POINT('Ctrl Pts',(-24.454095136893,20.4567884159491,-35.1793297560321));
#25419=CARTESIAN_POINT('Ctrl Pts',(-24.4365347497474,20.4517116619209,-35.1783083894944));
#25420=CARTESIAN_POINT('Ctrl Pts',(-24.3987638234237,20.4411393496812,-35.1761168222705));
#25421=CARTESIAN_POINT('Ctrl Pts',(-24.3785410076821,20.4356908627473,-35.1749466799054));
#25422=CARTESIAN_POINT('Ctrl Pts',(-24.334635900298,20.4243196856882,-35.1724109795536));
#25423=CARTESIAN_POINT('Ctrl Pts',(-24.3109365743327,20.4184681832578,-35.1710452212981));
#25424=CARTESIAN_POINT('Ctrl Pts',(-24.1904826768414,20.3901753541152,-35.1641107875761));
#25425=CARTESIAN_POINT('Ctrl Pts',(-24.0927979376789,20.3719471053991,-35.1585083961151));
#25426=CARTESIAN_POINT('Ctrl Pts',(-23.9056804910848,20.3459089518649,-35.1476476806953));
#25427=CARTESIAN_POINT('Ctrl Pts',(-23.8164595480765,20.3372665966226,-35.1424143933045));
#25428=CARTESIAN_POINT('Ctrl Pts',(-23.6813569010971,20.329845919941,-35.1343384349252));
#25429=CARTESIAN_POINT('Ctrl Pts',(-23.6356679660651,20.3283104188919,-35.1315815822287));
#25430=CARTESIAN_POINT('Ctrl Pts',(-23.5822167247633,20.3276517380722,-35.1283214795438));
#25431=CARTESIAN_POINT('Ctrl Pts',(-23.5744696488246,20.3275842095927,-35.1278481159485));
#25432=CARTESIAN_POINT('Ctrl Pts',(-23.5626375397355,20.3275237405816,-35.1271238199217));
#25433=CARTESIAN_POINT('Ctrl Pts',(-23.5585526008213,20.3275106310607,-35.1268735209531));
#25434=CARTESIAN_POINT('Ctrl Pts',(-23.5511230347141,20.3275009137005,-35.1264178409445));
#25435=CARTESIAN_POINT('Ctrl Pts',(-23.5477784118435,20.327501745851,-35.1262125405728));
#25436=CARTESIAN_POINT('Ctrl Pts',(-23.5410707265129,20.3275138567011,-35.1258004776397));
#25437=CARTESIAN_POINT('Ctrl Pts',(-23.5377076684354,20.3275251930705,-35.125593713523));
#25438=CARTESIAN_POINT('Ctrl Pts',(-23.528184908038,20.3275721991508,-35.1250077699927));
#25439=CARTESIAN_POINT('Ctrl Pts',(-23.5220253060965,20.3276202646386,-35.1246282018288));
#25440=CARTESIAN_POINT('Ctrl Pts',(-23.4962473305034,20.3278953302995,-35.1230373233066));
#25441=CARTESIAN_POINT('Ctrl Pts',(-23.4766314273234,20.3282838166514,-35.1218209540399));
#25442=CARTESIAN_POINT('Ctrl Pts',(-23.0687695973218,20.3400879134943,-35.0964055382194));
#25443=CARTESIAN_POINT('Ctrl Pts',(-22.6858002567252,20.4214309025551,-35.069623226068));
#25444=CARTESIAN_POINT('Ctrl Pts',(-22.2619159494658,20.5953907963724,-35.0391127391074));
#25445=CARTESIAN_POINT('Ctrl Pts',(-22.1980262642422,20.6240767824526,-35.0345060840688));
#25446=CARTESIAN_POINT('Ctrl Pts',(-22.1105750395999,20.6668183800062,-35.0282362718396));
#25447=CARTESIAN_POINT('Ctrl Pts',(-22.0861849470184,20.6791255736755,-35.0264916429329));
#25448=CARTESIAN_POINT('Ctrl Pts',(-22.0530367481557,20.6963843638634,-35.0241290368914));
#25449=CARTESIAN_POINT('Ctrl Pts',(-22.0441417376591,20.701068630269,-35.0234959003547));
#25450=CARTESIAN_POINT('Ctrl Pts',(-22.0310213396206,20.7080566720482,-35.0225634237095));
#25451=CARTESIAN_POINT('Ctrl Pts',(-22.0267790629514,20.7103283583577,-35.0222621421862));
#25452=CARTESIAN_POINT('Ctrl Pts',(-22.0191110044989,20.7144566348325,-35.0217179868206));
#25453=CARTESIAN_POINT('Ctrl Pts',(-22.0156834817916,20.7163099464567,-35.021474909191));
#25454=CARTESIAN_POINT('Ctrl Pts',(-22.0103520847799,20.7192052190653,-35.0210970582408));
#25455=CARTESIAN_POINT('Ctrl Pts',(-22.0084459023188,20.7202428867582,-35.0209620112815));
#25456=CARTESIAN_POINT('Ctrl Pts',(-22.0050664683966,20.7220869755354,-35.0207226789908));
#25457=CARTESIAN_POINT('Ctrl Pts',(-22.0035928052966,20.7228926193332,-35.0206183443167));
#25458=CARTESIAN_POINT('Ctrl Pts',(-22.0004661013168,20.7246051478809,-35.0203970398053));
#25459=CARTESIAN_POINT('Ctrl Pts',(-21.9988132312426,20.7255123286859,-35.0202800897926));
#25460=CARTESIAN_POINT('Ctrl Pts',(-21.9940976224202,20.7281058868451,-35.0199465399138));
#25461=CARTESIAN_POINT('Ctrl Pts',(-21.9910368184786,20.7297958050934,-35.0197301678666));
#25462=CARTESIAN_POINT('Ctrl Pts',(-21.9779407853439,20.7370541654883,-35.018804916382));
#25463=CARTESIAN_POINT('Ctrl Pts',(-21.9679324286924,20.742671299328,-35.0180991313007));
#25464=CARTESIAN_POINT('Ctrl Pts',(-21.7009309084297,20.8944056514917,-34.9992998452728));
#25465=CARTESIAN_POINT('Ctrl Pts',(-21.4651766638632,21.0751685348301,-34.9833461707932));
#25466=CARTESIAN_POINT('Ctrl Pts',(-21.2313806859363,21.3118787927702,-34.9646243229777));
#25467=CARTESIAN_POINT('Ctrl Pts',(-21.205862805503,21.338619568004,-34.9625369789373));
#25468=CARTESIAN_POINT('Ctrl Pts',(-21.147885086423,21.4015068943849,-34.957680125195));
#25469=CARTESIAN_POINT('Ctrl Pts',(-21.1157718935573,21.4379597179199,-34.9549029970278));
#25470=CARTESIAN_POINT('Ctrl Pts',(-21.0315754825357,21.5380054843777,-34.9473567351631));
#25471=CARTESIAN_POINT('Ctrl Pts',(-20.9810836477019,21.6028845899669,-34.9425411697672));
#25472=CARTESIAN_POINT('Ctrl Pts',(-20.9081159774944,21.7044277003997,-34.9350672818862));
#25473=CARTESIAN_POINT('Ctrl Pts',(-20.8838006839266,21.739730741519,-34.9324800478644));
#25474=CARTESIAN_POINT('Ctrl Pts',(-20.8560047646456,21.7818621618579,-34.9294014082383));
#25475=CARTESIAN_POINT('Ctrl Pts',(-20.85183453684,21.7882321419558,-34.9289361804053));
#25476=CARTESIAN_POINT('Ctrl Pts',(-20.8454771057194,21.7980185539106,-34.9282217808261));
#25477=CARTESIAN_POINT('Ctrl Pts',(-20.843273695402,21.8014244676805,-34.9279732159145));
#25478=CARTESIAN_POINT('Ctrl Pts',(-20.8394415001117,21.8073726650068,-34.9275392215435));
#25479=CARTESIAN_POINT('Ctrl Pts',(-20.8378098428642,21.809913099753,-34.9273538995561));
#25480=CARTESIAN_POINT('Ctrl Pts',(-20.8341473935797,21.8156330706004,-34.9269367084173));
#25481=CARTESIAN_POINT('Ctrl Pts',(-20.8321186124971,21.8188138832824,-34.9267047647537));
#25482=CARTESIAN_POINT('Ctrl Pts',(-20.8267059096458,21.8273331169293,-34.9260836792575));
#25483=CARTESIAN_POINT('Ctrl Pts',(-20.8233321122456,21.8326779227388,-34.925694162187));
#25484=CARTESIAN_POINT('Ctrl Pts',(-20.8088439040152,21.8557805871537,-34.9240110655563));
#25485=CARTESIAN_POINT('Ctrl Pts',(-20.7978872662342,21.8736363422054,-34.9227116708748));
#25486=CARTESIAN_POINT('Ctrl Pts',(-20.6049696973395,22.1950169192351,-34.8993459391184));
#25487=CARTESIAN_POINT('Ctrl Pts',(-20.4740912964217,22.5263137615742,-34.8752016316414));
#25488=CARTESIAN_POINT('Ctrl Pts',(-20.3857128622535,22.936900134127,-34.8469817843743));
#25489=CARTESIAN_POINT('Ctrl Pts',(-20.3737649936119,23.0021282267358,-34.8425601506712));
#25490=CARTESIAN_POINT('Ctrl Pts',(-20.355974417955,23.1195993131637,-34.8347545633238));
#25491=CARTESIAN_POINT('Ctrl Pts',(-20.3493811837904,23.1717050819643,-34.8313472464132));
#25492=CARTESIAN_POINT('Ctrl Pts',(-20.3423694219911,23.2406017471819,-34.8269337702772));
#25493=CARTESIAN_POINT('Ctrl Pts',(-20.3408046029275,23.2572650336904,-34.8258733933838));
#25494=CARTESIAN_POINT('Ctrl Pts',(-20.3387687088946,23.2809231032737,-34.8243786282739));
#25495=CARTESIAN_POINT('Ctrl Pts',(-20.3381905664341,23.2879080661663,-34.8239386293022));
#25496=CARTESIAN_POINT('Ctrl Pts',(-20.3373422496122,23.298580618528,-34.8232684216144));
#25497=CARTESIAN_POINT('Ctrl Pts',(-20.3370556310825,23.3022668248324,-34.8230373167542));
#25498=CARTESIAN_POINT('Ctrl Pts',(-20.3365960711801,23.3083118159932,-34.8226589595125));
#25499=CARTESIAN_POINT('Ctrl Pts',(-20.336419382582,23.3106702997338,-34.8225114988373));
#25500=CARTESIAN_POINT('Ctrl Pts',(-20.3360833331101,23.3152232433623,-34.8222271392617));
#25501=CARTESIAN_POINT('Ctrl Pts',(-20.3359236230253,23.3174176750563,-34.8220902207626));
#25502=CARTESIAN_POINT('Ctrl Pts',(-20.3356354306693,23.3214342783161,-34.8218398639653));
#25503=CARTESIAN_POINT('Ctrl Pts',(-20.3355062508854,23.3232563877852,-34.8217263866737));
#25504=CARTESIAN_POINT('Ctrl Pts',(-20.3352453232688,23.3269817278382,-34.8214945755224));
#25505=CARTESIAN_POINT('Ctrl Pts',(-20.3351137167087,23.328884958408,-34.8213762501168));
#25506=CARTESIAN_POINT('Ctrl Pts',(-20.3347381610182,23.3343870510235,-34.8210344784404));
#25507=CARTESIAN_POINT('Ctrl Pts',(-20.3344985629005,23.3379862219352,-34.8208112783485));
#25508=CARTESIAN_POINT('Ctrl Pts',(-20.3334599073399,23.3539940610067,-34.8198201715079));
#25509=CARTESIAN_POINT('Ctrl Pts',(-20.3327266114931,23.3664071071806,-34.8190559287683));
#25510=CARTESIAN_POINT('Ctrl Pts',(-20.3319161041495,23.3816225989949,-34.8181240698352));
#25511=CARTESIAN_POINT('Ctrl Pts',(-20.3317706932313,23.3844210790239,-34.8179528834798));
#25512=CARTESIAN_POINT('Ctrl Pts',(-20.3142344698232,23.7306244914373,-34.7968000507418));
#25513=CARTESIAN_POINT('Ctrl Pts',(-20.3519034369753,24.0746657812167,-34.778616175727));
#25514=CARTESIAN_POINT('Ctrl Pts',(-20.4803306509189,24.5407864827825,-34.7510381268298));
#25515=CARTESIAN_POINT('Ctrl Pts',(-20.5260739330218,24.6727115785153,-34.7429048886946));
#25516=CARTESIAN_POINT('Ctrl Pts',(-20.5886929379442,24.8213777837415,-34.7331551081335));
#25517=CARTESIAN_POINT('Ctrl Pts',(-20.5973757248957,24.8414198954033,-34.7318282207098));
#25518=CARTESIAN_POINT('Ctrl Pts',(-20.6087619989247,24.8669866687115,-34.7301189833596));
#25519=CARTESIAN_POINT('Ctrl Pts',(-20.6112786387176,24.8725943171394,-34.7297430609305));
#25520=CARTESIAN_POINT('Ctrl Pts',(-20.615349798928,24.8815967594228,-34.7291378904619));
#25521=CARTESIAN_POINT('Ctrl Pts',(-20.6168942122411,24.8849961299234,-34.7289089910469));
#25522=CARTESIAN_POINT('Ctrl Pts',(-20.6198404107847,24.8914511247411,-34.728473605495));
#25523=CARTESIAN_POINT('Ctrl Pts',(-20.6212410775153,24.8945072566315,-34.7282671582107));
#25524=CARTESIAN_POINT('Ctrl Pts',(-20.6244360282961,24.9014496577748,-34.7277974715753));
#25525=CARTESIAN_POINT('Ctrl Pts',(-20.6262332755181,24.9053345492541,-34.7275341299656));
#25526=CARTESIAN_POINT('Ctrl Pts',(-20.6317043343149,24.9170991098769,-34.7267351015627));
#25527=CARTESIAN_POINT('Ctrl Pts',(-20.6354022742847,24.9249674560404,-34.7261985790288));
#25528=CARTESIAN_POINT('Ctrl Pts',(-20.6712529042939,25.0004541551198,-34.7210307564238));
#25529=CARTESIAN_POINT('Ctrl Pts',(-20.7057186181147,25.0669426451405,-34.716319048056));
#25530=CARTESIAN_POINT('Ctrl Pts',(-20.7623389405108,25.1674397520354,-34.7089372048993));
#25531=CARTESIAN_POINT('Ctrl Pts',(-20.7828741488684,25.2023340546415,-34.7063239463006));
#25532=CARTESIAN_POINT('Ctrl Pts',(-20.9502315849255,25.4748358270205,-34.6855175868048));
#25533=CARTESIAN_POINT('Ctrl Pts',(-21.1267174429531,25.6928135061553,-34.6662983157725));
#25534=CARTESIAN_POINT('Ctrl Pts',(-21.3607907075178,25.9154788250315,-34.6447288517958));
#25535=CARTESIAN_POINT('Ctrl Pts',(-21.3931604229004,25.9450369510754,-34.6418223086919));
#25536=CARTESIAN_POINT('Ctrl Pts',(-21.4765051668817,26.0180809874363,-34.6345479490649));
#25537=CARTESIAN_POINT('Ctrl Pts',(-21.5282551540125,26.0606575881064,-34.6302209951882));
#25538=CARTESIAN_POINT('Ctrl Pts',(-21.5869984647487,26.1059917322859,-34.6255486880487));
#25539=CARTESIAN_POINT('Ctrl Pts',(-21.5927127125243,26.1103711327569,-34.6250966272968));
#25540=CARTESIAN_POINT('Ctrl Pts',(-21.6014415316638,26.1170145894063,-34.6244098463555));
#25541=CARTESIAN_POINT('Ctrl Pts',(-21.6044454340026,26.1192925301499,-34.6241741762029));
#25542=CARTESIAN_POINT('Ctrl Pts',(-21.609364676905,26.1230093481,-34.6237893523476));
#25543=CARTESIAN_POINT('Ctrl Pts',(-21.6112776262543,26.1244513618925,-34.6236399802311));
#25544=CARTESIAN_POINT('Ctrl Pts',(-21.6149669941101,26.1272260243948,-34.6233524285916));
#25545=CARTESIAN_POINT('Ctrl Pts',(-21.6167431847448,26.1285589718589,-34.6232142280549));
#25546=CARTESIAN_POINT('Ctrl Pts',(-21.6199838046169,26.1309856726019,-34.6229625179809));
#25547=CARTESIAN_POINT('Ctrl Pts',(-21.6214477812819,26.1320800120164,-34.6228489670848));
#25548=CARTESIAN_POINT('Ctrl Pts',(-21.6244297155514,26.1343050903757,-34.6226180063433));
#25549=CARTESIAN_POINT('Ctrl Pts',(-21.625947732553,26.1354357331815,-34.6225006033263));
#25550=CARTESIAN_POINT('Ctrl Pts',(-21.6303018593628,26.1386727948636,-34.6221643475704));
#25551=CARTESIAN_POINT('Ctrl Pts',(-21.6331404491474,26.1407758970027,-34.6219457286227));
#25552=CARTESIAN_POINT('Ctrl Pts',(-21.6454631027971,26.1498743649823,-34.6209992339244));
#25553=CARTESIAN_POINT('Ctrl Pts',(-21.6549821956541,26.1568224632323,-34.6202746306601));
#25554=CARTESIAN_POINT('Ctrl Pts',(-21.7949119147841,26.2577869817221,-34.6097151306432));
#25555=CARTESIAN_POINT('Ctrl Pts',(-21.9321291746763,26.3419599464169,-34.6005212020825));
#25556=CARTESIAN_POINT('Ctrl Pts',(-22.0750360449252,26.4155367897853,-34.591474087242));
#25557=CARTESIAN_POINT('Origin',(-23.5502525316942,23.5502525316942,-77.3107734492734));
#25558=CARTESIAN_POINT('',(-22.0750360001986,26.4155367667575,-33.0962096862788));
#25559=CARTESIAN_POINT('',(-22.0750360407426,26.4155367876319,-33.3457833635692));
#25560=CARTESIAN_POINT('',(-22.0750360153461,26.4155367745563,-77.3107734492734));
#25561=CARTESIAN_POINT('',(-26.7730025308237,23.5501776283632,-33.9361574895006));
#25562=CARTESIAN_POINT('Ctrl Pts',(-22.0750360001986,26.4155367667575,-33.0962096862788));
#25563=CARTESIAN_POINT('Ctrl Pts',(-21.8563691433369,26.3029542319481,-33.1099615826865));
#25564=CARTESIAN_POINT('Ctrl Pts',(-21.6513097234616,26.1657136843064,-33.1238651265134));
#25565=CARTESIAN_POINT('Ctrl Pts',(-21.4610347210246,26.0040862784072,-33.1390039367681));
#25566=CARTESIAN_POINT('Ctrl Pts',(-21.458232861277,26.0016979859802,-33.139227381038));
#25567=CARTESIAN_POINT('Ctrl Pts',(-21.4454577522704,25.9907706896878,-33.1402485665619));
#25568=CARTESIAN_POINT('Ctrl Pts',(-21.4355327586255,25.98217568352,-33.141048590918));
#25569=CARTESIAN_POINT('Ctrl Pts',(-21.422126419754,25.9704217213913,-33.1421384460553));
#25570=CARTESIAN_POINT('Ctrl Pts',(-21.4185989616122,25.9673153591477,-33.1424260810886));
#25571=CARTESIAN_POINT('Ctrl Pts',(-21.4126317063929,25.9620372316407,-33.1429141511737));
#25572=CARTESIAN_POINT('Ctrl Pts',(-21.41018838457,25.9598694468353,-33.1431144191584));
#25573=CARTESIAN_POINT('Ctrl Pts',(-21.4052881021335,25.9555084443362,-33.143516930587));
#25574=CARTESIAN_POINT('Ctrl Pts',(-21.4028312000315,25.9533151679095,-33.1437191763518));
#25575=CARTESIAN_POINT('Ctrl Pts',(-21.3972792591422,25.9483436367564,-33.1441771851765));
#25576=CARTESIAN_POINT('Ctrl Pts',(-21.3941862323565,25.9455631531174,-33.1444330421825));
#25577=CARTESIAN_POINT('Ctrl Pts',(-21.3877398969916,25.9397456025662,-33.1449677489944));
#25578=CARTESIAN_POINT('Ctrl Pts',(-21.3843875860916,25.9367074481065,-33.1452466446443));
#25579=CARTESIAN_POINT('Ctrl Pts',(-21.3756512876778,25.9287562876458,-33.1459756400078));
#25580=CARTESIAN_POINT('Ctrl Pts',(-21.3702775726531,25.9238320783085,-33.1464262164091));
#25581=CARTESIAN_POINT('Ctrl Pts',(-21.2571524504909,25.8194615404176,-33.155957739489));
#25582=CARTESIAN_POINT('Ctrl Pts',(-21.1563115625081,25.7128096071311,-33.1653543985603));
#25583=CARTESIAN_POINT('Ctrl Pts',(-20.9567632727159,25.4706398307789,-33.1860228294603));
#25584=CARTESIAN_POINT('Ctrl Pts',(-20.860646518114,25.3335318316986,-33.1973454138663));
#25585=CARTESIAN_POINT('Ctrl Pts',(-20.6802635049344,25.028228141126,-33.2213400399107));
#25586=CARTESIAN_POINT('Ctrl Pts',(-20.5991667660968,24.8588241884184,-33.2339646060946));
#25587=CARTESIAN_POINT('Ctrl Pts',(-20.5291905543973,24.6724982782971,-33.2465080515665));
#25588=CARTESIAN_POINT('Ctrl Pts',(-20.5251875538291,24.6616628410653,-33.2472327864698));
#25589=CARTESIAN_POINT('Ctrl Pts',(-20.520045867269,24.6475115798543,-33.2481729616063));
#25590=CARTESIAN_POINT('Ctrl Pts',(-20.5188542771561,24.644215268975,-33.2483915134105));
#25591=CARTESIAN_POINT('Ctrl Pts',(-20.5170293989265,24.6391412085909,-33.248727238891));
#25592=CARTESIAN_POINT('Ctrl Pts',(-20.516392295446,24.6373648491599,-33.2488446410119));
#25593=CARTESIAN_POINT('Ctrl Pts',(-20.5151287059076,24.6338319715404,-33.2490778724776));
#25594=CARTESIAN_POINT('Ctrl Pts',(-20.5145021877954,24.6320754792531,-33.2491937029656));
#25595=CARTESIAN_POINT('Ctrl Pts',(-20.5131084018173,24.6281571466912,-33.2494518082576));
#25596=CARTESIAN_POINT('Ctrl Pts',(-20.5123419191119,24.6259950356032,-33.2495940353704));
#25597=CARTESIAN_POINT('Ctrl Pts',(-20.5101086582739,24.6196739825514,-33.2500092833688));
#25598=CARTESIAN_POINT('Ctrl Pts',(-20.5086480999534,24.6155128247743,-33.2502819325762));
#25599=CARTESIAN_POINT('Ctrl Pts',(-20.4981266829518,24.5853390589097,-33.2522539461489));
#25600=CARTESIAN_POINT('Ctrl Pts',(-20.4893907575546,24.5592132037144,-33.2539342641068));
#25601=CARTESIAN_POINT('Ctrl Pts',(-20.4626942376948,24.4758342157061,-33.2592205597368));
#25602=CARTESIAN_POINT('Ctrl Pts',(-20.4459960859557,24.4181871849207,-33.2627620246941));
#25603=CARTESIAN_POINT('Ctrl Pts',(-20.4039763335248,24.2563380369206,-33.272477228195));
#25604=CARTESIAN_POINT('Ctrl Pts',(-20.3822291417035,24.1512860302444,-33.2785255360439));
#25605=CARTESIAN_POINT('Ctrl Pts',(-20.3305533520322,23.8188976170506,-33.2973760650303));
#25606=CARTESIAN_POINT('Ctrl Pts',(-20.3196031291299,23.5893648384889,-33.3100296851615));
#25607=CARTESIAN_POINT('Ctrl Pts',(-20.3356199569554,23.3176406636581,-33.3259475145926));
#25608=CARTESIAN_POINT('Ctrl Pts',(-20.3390139194764,23.274721766108,-33.3284876399393));
#25609=CARTESIAN_POINT('Ctrl Pts',(-20.3435644573659,23.2288831854638,-33.331233243591));
#25610=CARTESIAN_POINT('Ctrl Pts',(-20.3438666796838,23.2258817089097,-33.331413173534));
#25611=CARTESIAN_POINT('Ctrl Pts',(-20.3487237541363,23.1783144981107,-33.3342670892068));
#25612=CARTESIAN_POINT('Ctrl Pts',(-20.3542029487011,23.1338498771441,-33.3369683206224));
#25613=CARTESIAN_POINT('Ctrl Pts',(-20.3617678339112,23.081478778588,-33.3401940811659));
#25614=CARTESIAN_POINT('Ctrl Pts',(-20.3629590867119,23.0734464985223,-33.3406900538544));
#25615=CARTESIAN_POINT('Ctrl Pts',(-20.3648204958809,23.0612142965102,-33.3414472648864));
#25616=CARTESIAN_POINT('Ctrl Pts',(-20.365468636815,23.0570110159026,-33.3417078038659));
#25617=CARTESIAN_POINT('Ctrl Pts',(-20.3666328507282,23.0495589020947,-33.3421703336049));
#25618=CARTESIAN_POINT('Ctrl Pts',(-20.367145582272,23.046309546657,-33.3423722179013));
#25619=CARTESIAN_POINT('Ctrl Pts',(-20.3682380853729,23.0394541708399,-33.3427985852264));
#25620=CARTESIAN_POINT('Ctrl Pts',(-20.3688190134011,23.0358483418249,-33.343023104774));
#25621=CARTESIAN_POINT('Ctrl Pts',(-20.3700195596786,23.0284763593021,-33.3434826542821));
#25622=CARTESIAN_POINT('Ctrl Pts',(-20.3706397411729,23.0247103045379,-33.3437177018581));
#25623=CARTESIAN_POINT('Ctrl Pts',(-20.3721875351231,23.0154143501939,-33.3442985825956));
#25624=CARTESIAN_POINT('Ctrl Pts',(-20.373122889533,23.0098857682043,-33.3446446620109));
#25625=CARTESIAN_POINT('Ctrl Pts',(-20.3825415490207,22.9550849831333,-33.3480812172106));
#25626=CARTESIAN_POINT('Ctrl Pts',(-20.3921555295228,22.9060164325008,-33.3512075851869));
#25627=CARTESIAN_POINT('Ctrl Pts',(-20.427173596164,22.7469910612913,-33.3615087445516));
#25628=CARTESIAN_POINT('Ctrl Pts',(-20.4572092184017,22.6381509536648,-33.3688281669958));
#25629=CARTESIAN_POINT('Ctrl Pts',(-20.5750435148632,22.2846519901156,-33.3934676448708));
#25630=CARTESIAN_POINT('Ctrl Pts',(-20.6866906506669,22.0490497753747,-33.4113898685815));
#25631=CARTESIAN_POINT('Ctrl Pts',(-20.873256927838,21.7536318750307,-33.4344967022571));
#25632=CARTESIAN_POINT('Ctrl Pts',(-20.9242628469046,21.6798694394627,-33.4403153220695));
#25633=CARTESIAN_POINT('Ctrl Pts',(-20.9821442319796,21.6032090350653,-33.4463371357854));
#25634=CARTESIAN_POINT('Ctrl Pts',(-20.9860203934933,21.5981070043533,-33.4467377807296));
#25635=CARTESIAN_POINT('Ctrl Pts',(-20.9914159621467,21.5910488395923,-33.4472918152884));
#25636=CARTESIAN_POINT('Ctrl Pts',(-20.9929224135749,21.5890828899089,-33.4474461099586));
#25637=CARTESIAN_POINT('Ctrl Pts',(-20.9955152272929,21.5857072827187,-33.447710995998));
#25638=CARTESIAN_POINT('Ctrl Pts',(-20.9966004906228,21.5842967888202,-33.4478216652609));
#25639=CARTESIAN_POINT('Ctrl Pts',(-20.9988443152639,21.5813855300486,-33.4480500582407));
#25640=CARTESIAN_POINT('Ctrl Pts',(-21.0000030303393,21.5798848914072,-33.4481677699938));
#25641=CARTESIAN_POINT('Ctrl Pts',(-21.002725924987,21.5763649272631,-33.4484438447483));
#25642=CARTESIAN_POINT('Ctrl Pts',(-21.0042911863621,21.574346431954,-33.4486021305158));
#25643=CARTESIAN_POINT('Ctrl Pts',(-21.0093797040153,21.5678005786252,-33.4491153610684));
#25644=CARTESIAN_POINT('Ctrl Pts',(-21.0129126750462,21.5632807337739,-33.4494696167201));
#25645=CARTESIAN_POINT('Ctrl Pts',(-21.1113438648524,21.4380451509746,-33.4592825933531));
#25646=CARTESIAN_POINT('Ctrl Pts',(-21.2147521873465,21.3242363460958,-33.4681333878435));
#25647=CARTESIAN_POINT('Ctrl Pts',(-21.4055294426812,21.142267750801,-33.483030971068));
#25648=CARTESIAN_POINT('Ctrl Pts',(-21.4890004342668,21.0704403289412,-33.4891509524939));
#25649=CARTESIAN_POINT('Ctrl Pts',(-21.5829023043167,20.9976602670516,-33.4957978756344));
#25650=CARTESIAN_POINT('Ctrl Pts',(-21.5898428124929,20.9923260434801,-33.4962878113997));
#25651=CARTESIAN_POINT('Ctrl Pts',(-21.6775652021031,20.9254725299975,-33.5024640968307));
#25652=CARTESIAN_POINT('Ctrl Pts',(-21.7611859506289,20.8677784600446,-33.5081824841757));
#25653=CARTESIAN_POINT('Ctrl Pts',(-21.9614576917328,20.7431364532308,-33.5217229239747));
#25654=CARTESIAN_POINT('Ctrl Pts',(-22.0798423872788,20.6793542897056,-33.5296175284711));
#25655=CARTESIAN_POINT('Ctrl Pts',(-22.211787265767,20.6185724728253,-33.5384551188689));
#25656=CARTESIAN_POINT('Ctrl Pts',(-22.2217463673485,20.6140460331101,-33.539122349422));
#25657=CARTESIAN_POINT('Ctrl Pts',(-22.235696797289,20.6077910282131,-33.540057298118));
#25658=CARTESIAN_POINT('Ctrl Pts',(-22.2396689504383,20.6060196681852,-33.5403235442553));
#25659=CARTESIAN_POINT('Ctrl Pts',(-22.2465439899483,20.6029704514811,-33.5407844308286));
#25660=CARTESIAN_POINT('Ctrl Pts',(-22.2494452070051,20.6016888260753,-33.5409789416953));
#25661=CARTESIAN_POINT('Ctrl Pts',(-22.2554004527121,20.5990685701119,-33.541378251856));
#25662=CARTESIAN_POINT('Ctrl Pts',(-22.2584546751475,20.5977303930413,-33.5415830663621));
#25663=CARTESIAN_POINT('Ctrl Pts',(-22.265574740991,20.5946239700525,-33.5420605910396));
#25664=CARTESIAN_POINT('Ctrl Pts',(-22.2696421601395,20.5928593728006,-33.5423334256436));
#25665=CARTESIAN_POINT('Ctrl Pts',(-22.2782159273906,20.5891607588091,-33.5429086337005));
#25666=CARTESIAN_POINT('Ctrl Pts',(-22.282723070723,20.5872286243859,-33.5432110707151));
#25667=CARTESIAN_POINT('Ctrl Pts',(-22.2947771836881,20.5820937712283,-33.544020080544));
#25668=CARTESIAN_POINT('Ctrl Pts',(-22.3023319571902,20.5789095668862,-33.5445272834179));
#25669=CARTESIAN_POINT('Ctrl Pts',(-22.4648403612685,20.5111442177498,-33.5554414300634));
#25670=CARTESIAN_POINT('Ctrl Pts',(-22.624566872141,20.4587498784554,-33.5662651477506));
#25671=CARTESIAN_POINT('Ctrl Pts',(-23.0510544832198,20.3548760843953,-33.5953898869025));
#25672=CARTESIAN_POINT('Ctrl Pts',(-23.3215040707769,20.3242192657087,-33.6141478595023));
#25673=CARTESIAN_POINT('Ctrl Pts',(-23.6027828106135,20.327914546034,-33.6325635426624));
#25674=CARTESIAN_POINT('Ctrl Pts',(-23.6129775065822,20.3280968703002,-33.6332293528822));
#25675=CARTESIAN_POINT('Ctrl Pts',(-23.6269571924176,20.328413259163,-33.6341399499521));
#25676=CARTESIAN_POINT('Ctrl Pts',(-23.6307429668876,20.3285056153361,-33.6343863022404));
#25677=CARTESIAN_POINT('Ctrl Pts',(-23.6887480650497,20.3300229881183,-33.6381570791507));
#25678=CARTESIAN_POINT('Ctrl Pts',(-23.7429272447251,20.3328099671841,-33.6416283943474));
#25679=CARTESIAN_POINT('Ctrl Pts',(-23.8022101889767,20.3373625460055,-33.6453525066291));
#25680=CARTESIAN_POINT('Ctrl Pts',(-23.8074053589227,20.3377741822644,-33.6456782367516));
#25681=CARTESIAN_POINT('Ctrl Pts',(-23.8151110842944,20.3384035533805,-33.6461604223376));
#25682=CARTESIAN_POINT('Ctrl Pts',(-23.8176223870372,20.3386116313225,-33.6463174168352));
#25683=CARTESIAN_POINT('Ctrl Pts',(-23.8219184263796,20.3389726602417,-33.646585724408));
#25684=CARTESIAN_POINT('Ctrl Pts',(-23.8237032789949,20.3391241536987,-33.6466971199233));
#25685=CARTESIAN_POINT('Ctrl Pts',(-23.8271823139483,20.3394223664628,-33.6469141011146));
#25686=CARTESIAN_POINT('Ctrl Pts',(-23.8288765018063,20.3395689381976,-33.6470196946127));
#25687=CARTESIAN_POINT('Ctrl Pts',(-23.8329687540999,20.3399262406164,-33.6472745843194));
#25688=CARTESIAN_POINT('Ctrl Pts',(-23.8353667051238,20.3401383178698,-33.647423803846));
#25689=CARTESIAN_POINT('Ctrl Pts',(-23.8427093881134,20.3407960047309,-33.647880304045));
#25690=CARTESIAN_POINT('Ctrl Pts',(-23.8476533596564,20.3412503566181,-33.6481870914634));
#25691=CARTESIAN_POINT('Ctrl Pts',(-23.8991286391414,20.3461009264995,-33.6513753883521));
#25692=CARTESIAN_POINT('Ctrl Pts',(-23.9455631103241,20.3514977492686,-33.6542013405379));
#25693=CARTESIAN_POINT('Ctrl Pts',(-24.0797102778871,20.3700550183086,-33.6622623549987));
#25694=CARTESIAN_POINT('Ctrl Pts',(-24.1670220117896,20.385828477111,-33.6673810797301));
#25695=CARTESIAN_POINT('Ctrl Pts',(-24.4595869022026,20.4512542135287,-33.6844254629808));
#25696=CARTESIAN_POINT('Ctrl Pts',(-24.6605722014291,20.517452757095,-33.6959852887159));
#25697=CARTESIAN_POINT('Ctrl Pts',(-25.0021907254882,20.6685214525579,-33.7172273695192));
#25698=CARTESIAN_POINT('Ctrl Pts',(-25.1455374519714,20.7453366397997,-33.7266900189917));
#25699=CARTESIAN_POINT('Ctrl Pts',(-25.2920499245774,20.8387237399306,-33.7372566753492));
#25700=CARTESIAN_POINT('Ctrl Pts',(-25.3015945470176,20.8448786783058,-33.7379492432885));
#25701=CARTESIAN_POINT('Ctrl Pts',(-25.3148079174917,20.8534986708749,-33.7389139443849));
#25702=CARTESIAN_POINT('Ctrl Pts',(-25.3185045074394,20.8559210663123,-33.7391844785292));
#25703=CARTESIAN_POINT('Ctrl Pts',(-25.3248607686757,20.8601050738654,-33.7396507825216));
#25704=CARTESIAN_POINT('Ctrl Pts',(-25.3275228359763,20.8618630500468,-33.7398464155035));
#25705=CARTESIAN_POINT('Ctrl Pts',(-25.3329533086972,20.8654608170367,-33.7402461934387));
#25706=CARTESIAN_POINT('Ctrl Pts',(-25.3357214856984,20.8673009433165,-33.7404503508605));
#25707=CARTESIAN_POINT('Ctrl Pts',(-25.3421223107855,20.871570140324,-33.7409232843133));
#25708=CARTESIAN_POINT('Ctrl Pts',(-25.3457528686692,20.8740023194234,-33.7411921776042));
#25709=CARTESIAN_POINT('Ctrl Pts',(-25.3533735968306,20.8791300757595,-33.7417579607111));
#25710=CARTESIAN_POINT('Ctrl Pts',(-25.3573626919273,20.8818272247923,-33.7420549097481));
#25711=CARTESIAN_POINT('Ctrl Pts',(-25.3679508446266,20.889020829745,-33.7428452003928));
#25712=CARTESIAN_POINT('Ctrl Pts',(-25.3745392294246,20.8935328680983,-33.7433391342962));
#25713=CARTESIAN_POINT('Ctrl Pts',(-25.5153070280779,20.9907078582783,-33.7539397125554));
#25714=CARTESIAN_POINT('Ctrl Pts',(-25.6422567166878,21.09338224976,-33.7644389256691));
#25715=CARTESIAN_POINT('Ctrl Pts',(-25.9895662079937,21.4207834984232,-33.7960580255962));
#25716=CARTESIAN_POINT('Ctrl Pts',(-26.185470304081,21.668630730991,-33.8179760209795));
#25717=CARTESIAN_POINT('Ctrl Pts',(-26.3451220011464,21.9456180217913,-33.8384547718852));
#25718=CARTESIAN_POINT('Ctrl Pts',(-26.3478314730971,21.9503464940923,-33.8388032263949));
#25719=CARTESIAN_POINT('Ctrl Pts',(-26.3528853098807,21.9592183597707,-33.8394548545913));
#25720=CARTESIAN_POINT('Ctrl Pts',(-26.3552325098241,21.9633601129969,-33.839758181165));
#25721=CARTESIAN_POINT('Ctrl Pts',(-26.3608358495007,21.9732987650764,-33.8404839161433));
#25722=CARTESIAN_POINT('Ctrl Pts',(-26.3640832599876,21.979100596782,-33.8409058391203));
#25723=CARTESIAN_POINT('Ctrl Pts',(-26.3753322015171,21.9993447255904,-33.8423718962414));
#25724=CARTESIAN_POINT('Ctrl Pts',(-26.3832408587141,22.0138387428455,-33.8434106793214));
#25725=CARTESIAN_POINT('Ctrl Pts',(-26.392742758226,22.0315755062785,-33.8446680972323));
#25726=CARTESIAN_POINT('Ctrl Pts',(-26.3944422040401,22.0347606302013,-33.8448933631846));
#25727=CARTESIAN_POINT('Ctrl Pts',(-26.3972309081421,22.0400084694065,-33.8452636200412));
#25728=CARTESIAN_POINT('Ctrl Pts',(-26.3983232791431,22.0420695118871,-33.8454088087808));
#25729=CARTESIAN_POINT('Ctrl Pts',(-26.4002861671601,22.0457827491069,-33.8456699753775));
#25730=CARTESIAN_POINT('Ctrl Pts',(-26.4011574838513,22.0474345108309,-33.845786004319));
#25731=CARTESIAN_POINT('Ctrl Pts',(-26.4030250904985,22.050982416565,-33.8460349153433));
#25732=CARTESIAN_POINT('Ctrl Pts',(-26.4040209232339,22.0528787914746,-33.8461677678749));
#25733=CARTESIAN_POINT('Ctrl Pts',(-26.406735822555,22.0580613490185,-33.8465303177134));
#25734=CARTESIAN_POINT('Ctrl Pts',(-26.4084511152392,22.0613495214307,-33.8467597743161));
#25735=CARTESIAN_POINT('Ctrl Pts',(-26.4172315678012,22.078252515367,-33.8479364185784));
#25736=CARTESIAN_POINT('Ctrl Pts',(-26.4242052938448,22.0919149903348,-33.8488778769539));
#25737=CARTESIAN_POINT('Ctrl Pts',(-26.4888348947098,22.2207974037022,-33.8576738508968));
#25738=CARTESIAN_POINT('Ctrl Pts',(-26.5396376523674,22.3393428356898,-33.8651296980488));
#25739=CARTESIAN_POINT('Ctrl Pts',(-26.6985628855833,22.7817085554313,-33.8917933600327));
#25740=CARTESIAN_POINT('Ctrl Pts',(-26.7621954688444,23.119040749908,-33.9102126580092));
#25741=CARTESIAN_POINT('Ctrl Pts',(-26.7723407741092,23.4815171997508,-33.9319943926306));
#25742=CARTESIAN_POINT('Ctrl Pts',(-26.7727267181171,23.5029527245104,-33.933288605986));
#25743=CARTESIAN_POINT('Ctrl Pts',(-26.7729677403501,23.5329858601504,-33.9351110803763));
#25744=CARTESIAN_POINT('Ctrl Pts',(-26.7730023310382,23.5415817653069,-33.9356337488379));
#25745=CARTESIAN_POINT('Ctrl Pts',(-26.7730025308237,23.5501776283632,-33.9361574895006));
#25746=CARTESIAN_POINT('Ctrl Pts',(-26.7730025308395,23.550178309149,-33.9361575309805));
#25747=CARTESIAN_POINT('Ctrl Pts',(-26.7730026748028,23.5564292106473,-33.9365383946152));
#25748=CARTESIAN_POINT('Ctrl Pts',(-26.7729846322319,23.5626800735835,-33.936919824221));
#25749=CARTESIAN_POINT('Ctrl Pts',(-26.7729246733282,23.5730252035013,-33.9375520422594));
#25750=CARTESIAN_POINT('Ctrl Pts',(-26.7728931401916,23.5771195237905,-33.9378025044864));
#25751=CARTESIAN_POINT('Ctrl Pts',(-26.7728227214832,23.5844490596819,-33.9382513222316));
#25752=CARTESIAN_POINT('Ctrl Pts',(-26.7727867662673,23.587684303309,-33.9384495856059));
#25753=CARTESIAN_POINT('Ctrl Pts',(-26.7727045033626,23.594202906064,-33.9388493776558));
#25754=CARTESIAN_POINT('Ctrl Pts',(-26.7726580493122,23.5974862591902,-33.9390509106868));
#25755=CARTESIAN_POINT('Ctrl Pts',(-26.7725550984058,23.6040532427504,-33.9394543198279));
#25756=CARTESIAN_POINT('Ctrl Pts',(-26.772498600233,23.6073368693641,-33.9396561957481));
#25757=CARTESIAN_POINT('Ctrl Pts',(-26.7723290392965,23.6163873244561,-33.9402130662241));
#25758=CARTESIAN_POINT('Ctrl Pts',(-26.7722055140904,23.6221539238401,-33.9405683889328));
#25759=CARTESIAN_POINT('Ctrl Pts',(-26.7716646389071,23.6445905543983,-33.9419528676441));
#25760=CARTESIAN_POINT('Ctrl Pts',(-26.7711333957747,23.6612573496447,-33.9429855938912));
#25761=CARTESIAN_POINT('Ctrl Pts',(-26.7673121293714,23.7576437976958,-33.9489834629668));
#25762=CARTESIAN_POINT('Ctrl Pts',(-26.7611921072332,23.8372173575544,-33.9540369670017));
#25763=CARTESIAN_POINT('Ctrl Pts',(-26.7160170114568,24.2321804174524,-33.9796545483204));
#25764=CARTESIAN_POINT('Ctrl Pts',(-26.633410184405,24.540788258247,-34.0016150782062));
#25765=CARTESIAN_POINT('Ctrl Pts',(-26.4697526943507,24.9182538998597,-34.0289546906226));
#25766=CARTESIAN_POINT('Ctrl Pts',(-26.4287144057312,25.0026195295785,-34.0350797575828));
#25767=CARTESIAN_POINT('Ctrl Pts',(-26.3777406275214,25.0967337583122,-34.0418341268903));
#25768=CARTESIAN_POINT('Ctrl Pts',(-26.3713585680126,25.1083455528806,-34.0426660560792));
#25769=CARTESIAN_POINT('Ctrl Pts',(-26.3631864848201,25.1229993601418,-34.0437138016294));
#25770=CARTESIAN_POINT('Ctrl Pts',(-26.3614629547836,25.1260780196333,-34.0439338057856));
#25771=CARTESIAN_POINT('Ctrl Pts',(-26.3587047030692,25.1309860261931,-34.0442843381788));
#25772=CARTESIAN_POINT('Ctrl Pts',(-26.3576732480507,25.1328171910255,-34.0444150766871));
#25773=CARTESIAN_POINT('Ctrl Pts',(-26.3557189380392,25.136278797346,-34.0446621371332));
#25774=CARTESIAN_POINT('Ctrl Pts',(-26.3547964593768,25.1379094310856,-34.0447784818508));
#25775=CARTESIAN_POINT('Ctrl Pts',(-26.3526914965804,25.1416227420244,-34.0450433429258));
#25776=CARTESIAN_POINT('Ctrl Pts',(-26.3515081143427,25.1437049028126,-34.045191799973));
#25777=CARTESIAN_POINT('Ctrl Pts',(-26.3484350510253,25.1490979538069,-34.0455761760316));
#25778=CARTESIAN_POINT('Ctrl Pts',(-26.3465418081482,25.1524068245231,-34.0458118647498));
#25779=CARTESIAN_POINT('Ctrl Pts',(-26.3350489188892,25.1724108235579,-34.0472359206745));
#25780=CARTESIAN_POINT('Ctrl Pts',(-26.3253053869441,25.1890234539341,-34.0484151055922));
#25781=CARTESIAN_POINT('Ctrl Pts',(-26.3131335552557,25.2093564197911,-34.0498553703653));
#25782=CARTESIAN_POINT('Ctrl Pts',(-26.3108459915708,25.2131599288851,-34.0501246581064));
#25783=CARTESIAN_POINT('Ctrl Pts',(-26.3067079486234,25.2200081399085,-34.0506092983583));
#25784=CARTESIAN_POINT('Ctrl Pts',(-26.3048602691497,25.2230545132971,-34.0508248109953));
#25785=CARTESIAN_POINT('Ctrl Pts',(-26.299939908391,25.2311367316886,-34.0513963951882));
#25786=CARTESIAN_POINT('Ctrl Pts',(-26.2968584294008,25.2361672410247,-34.0517519684595));
#25787=CARTESIAN_POINT('Ctrl Pts',(-26.1289376339257,25.5086153246693,-34.0710007669192));
#25788=CARTESIAN_POINT('Ctrl Pts',(-25.9258736091611,25.7505463979685,-34.0877711919136));
#25789=CARTESIAN_POINT('Ctrl Pts',(-25.5795725474262,26.058277027856,-34.1141110341939));
#25790=CARTESIAN_POINT('Ctrl Pts',(-25.4614555783776,26.1494102511916,-34.1227719060809));
#25791=CARTESIAN_POINT('Ctrl Pts',(-25.3250524106673,26.2403130448343,-34.1326742769969));
#25792=CARTESIAN_POINT('Ctrl Pts',(-25.3125795402053,26.2485007927453,-34.1335787766699));
#25793=CARTESIAN_POINT('Ctrl Pts',(-25.2937196724821,26.2606946956066,-34.1349451683691));
#25794=CARTESIAN_POINT('Ctrl Pts',(-25.2873746209282,26.264765607828,-34.1354046497046));
#25795=CARTESIAN_POINT('Ctrl Pts',(-25.2771105719835,26.2713001789964,-34.1361476057685));
#25796=CARTESIAN_POINT('Ctrl Pts',(-25.273200422461,26.2737777391324,-34.1364305641104));
#25797=CARTESIAN_POINT('Ctrl Pts',(-25.2657028320924,26.2785057757598,-34.136972990861));
#25798=CARTESIAN_POINT('Ctrl Pts',(-25.2621162641396,26.280757623826,-34.1372324077716));
#25799=CARTESIAN_POINT('Ctrl Pts',(-25.2557236603312,26.2847537125509,-34.1376946836892));
#25800=CARTESIAN_POINT('Ctrl Pts',(-25.2529193558775,26.2865007229983,-34.1378974398654));
#25801=CARTESIAN_POINT('Ctrl Pts',(-25.2473632567401,26.2899501829263,-34.1382990891161));
#25802=CARTESIAN_POINT('Ctrl Pts',(-25.2446115742029,26.2916528067677,-34.1384979754543));
#25803=CARTESIAN_POINT('Ctrl Pts',(-25.2379510153503,26.2957602175558,-34.1389793125636));
#25804=CARTESIAN_POINT('Ctrl Pts',(-25.2340395652403,26.2981607998471,-34.1392619178657));
#25805=CARTESIAN_POINT('Ctrl Pts',(-25.2195356375732,26.3070197300616,-34.1403096170406));
#25806=CARTESIAN_POINT('Ctrl Pts',(-25.2089111273498,26.3134251882087,-34.1410766496949));
#25807=CARTESIAN_POINT('Ctrl Pts',(-25.0239503714321,26.4234858634406,-34.1544232022468));
#25808=CARTESIAN_POINT('Ctrl Pts',(-24.8402839014482,26.5104967788181,-34.1676195293596));
#25809=CARTESIAN_POINT('Ctrl Pts',(-24.3728094877983,26.6801534362199,-34.2009236013512));
#25810=CARTESIAN_POINT('Ctrl Pts',(-24.0834569296122,26.7422086947903,-34.2213678720136));
#25811=CARTESIAN_POINT('Ctrl Pts',(-23.7767855565863,26.7650570357422,-34.2407691063148));
#25812=CARTESIAN_POINT('Ctrl Pts',(-23.7638675013172,26.7659412400283,-34.2415819518618));
#25813=CARTESIAN_POINT('Ctrl Pts',(-23.747451102101,26.766965533445,-34.2426090353967));
#25814=CARTESIAN_POINT('Ctrl Pts',(-23.7439576219611,26.7671777950607,-34.2428272645952));
#25815=CARTESIAN_POINT('Ctrl Pts',(-23.7383721105015,26.7675080355294,-34.2431756291451));
#25816=CARTESIAN_POINT('Ctrl Pts',(-23.7362803104675,26.7676296650862,-34.2433059702763));
#25817=CARTESIAN_POINT('Ctrl Pts',(-23.7323167027201,26.7678562541523,-34.2435527097234));
#25818=CARTESIAN_POINT('Ctrl Pts',(-23.730444935898,26.7679616196375,-34.2436691299855));
#25819=CARTESIAN_POINT('Ctrl Pts',(-23.7261708599775,26.7681984747732,-34.2439347432902));
#25820=CARTESIAN_POINT('Ctrl Pts',(-23.7237684984537,26.7683289074465,-34.2440838757663));
#25821=CARTESIAN_POINT('Ctrl Pts',(-23.7164153258074,26.7687198791526,-34.2445398499783));
#25822=CARTESIAN_POINT('Ctrl Pts',(-23.7114640279032,26.7689716861206,-34.244846200119));
#25823=CARTESIAN_POINT('Ctrl Pts',(-23.6923081619518,26.7699015791108,-34.2460288530424));
#25824=CARTESIAN_POINT('Ctrl Pts',(-23.6780994798894,26.7704970823297,-34.2469006047019));
#25825=CARTESIAN_POINT('Ctrl Pts',(-23.33974970073,26.782434752341,-34.2675392045379));
#25826=CARTESIAN_POINT('Ctrl Pts',(-23.0156821232511,26.7448780214831,-34.2848212851987));
#25827=CARTESIAN_POINT('Ctrl Pts',(-22.5521582334988,26.6185178297042,-34.3120772832817));
#25828=CARTESIAN_POINT('Ctrl Pts',(-22.4048753521352,26.5666320858267,-34.3211204643152));
#25829=CARTESIAN_POINT('Ctrl Pts',(-22.2479278794801,26.4981842970364,-34.3314608809321));
#25830=CARTESIAN_POINT('Ctrl Pts',(-22.233961182635,26.4919745214214,-34.3323872762318));
#25831=CARTESIAN_POINT('Ctrl Pts',(-22.2130498014579,26.4824983104864,-34.3337838692999));
#25832=CARTESIAN_POINT('Ctrl Pts',(-22.2060716142644,26.4793059809532,-34.3342515263368));
#25833=CARTESIAN_POINT('Ctrl Pts',(-22.1948511522685,26.4741243853716,-34.3350061115167));
#25834=CARTESIAN_POINT('Ctrl Pts',(-22.1906016691858,26.4721507242724,-34.3352925010232));
#25835=CARTESIAN_POINT('Ctrl Pts',(-22.1824824919245,26.4683582466141,-34.3358408559628));
#25836=CARTESIAN_POINT('Ctrl Pts',(-22.1786120809899,26.4665409808796,-34.3361027672922));
#25837=CARTESIAN_POINT('Ctrl Pts',(-22.171752231356,26.4633034132402,-34.336567885651));
#25838=CARTESIAN_POINT('Ctrl Pts',(-22.1687613366919,26.4618861958949,-34.3367709853125));
#25839=CARTESIAN_POINT('Ctrl Pts',(-22.162864093755,26.4590806907645,-34.3371720539694));
#25840=CARTESIAN_POINT('Ctrl Pts',(-22.1599576324459,26.4576926479692,-34.337370014267));
#25841=CARTESIAN_POINT('Ctrl Pts',(-22.1529644565345,26.4543400232102,-34.3378470315061));
#25842=CARTESIAN_POINT('Ctrl Pts',(-22.1488798057749,26.4523711726333,-34.3381262370635));
#25843=CARTESIAN_POINT('Ctrl Pts',(-22.1363532599769,26.4463006151483,-34.3389842902274));
#25844=CARTESIAN_POINT('Ctrl Pts',(-22.127925173531,26.4421706729057,-34.3395641235328));
#25845=CARTESIAN_POINT('Ctrl Pts',(-22.1046298374322,26.4306289926365,-34.3411738468377));
#25846=CARTESIAN_POINT('Ctrl Pts',(-22.0898029703684,26.4231396698567,-34.3422063933191));
#25847=CARTESIAN_POINT('Ctrl Pts',(-22.0750360068226,26.4155367701679,-34.3432429022327));
#25848=CARTESIAN_POINT('Ctrl Pts',(-22.0750360449252,26.4155367897853,-34.591474087242));
#25849=CARTESIAN_POINT('Ctrl Pts',(-22.0989250851324,26.4278362696248,-34.5899617254513));
#25850=CARTESIAN_POINT('Ctrl Pts',(-22.1229731237522,26.4398396576589,-34.5884536415116));
#25851=CARTESIAN_POINT('Ctrl Pts',(-22.3062474010362,26.5284719415273,-34.5770499000293));
#25852=CARTESIAN_POINT('Ctrl Pts',(-22.4713701982389,26.5921844381592,-34.5672641465516));
#25853=CARTESIAN_POINT('Ctrl Pts',(-22.7597642822913,26.6770083710693,-34.550017748628));
#25854=CARTESIAN_POINT('Ctrl Pts',(-22.8805536989833,26.7050856179438,-34.5427550083098));
#25855=CARTESIAN_POINT('Ctrl Pts',(-23.0226937761657,26.72959413185,-34.5340299418283));
#25856=CARTESIAN_POINT('Ctrl Pts',(-23.0427692406262,26.7328602566257,-34.5327937048404));
#25857=CARTESIAN_POINT('Ctrl Pts',(-23.0687953944981,26.7368420051045,-34.5311855281455));
#25858=CARTESIAN_POINT('Ctrl Pts',(-23.0747193465569,26.7377314157142,-34.5308191148241));
#25859=CARTESIAN_POINT('Ctrl Pts',(-23.0843050369607,26.7391432754798,-34.5302256063493));
#25860=CARTESIAN_POINT('Ctrl Pts',(-23.087965274411,26.739675949057,-34.5299988359311));
#25861=CARTESIAN_POINT('Ctrl Pts',(-23.0949620081948,26.7406818849192,-34.5295650764876));
#25862=CARTESIAN_POINT('Ctrl Pts',(-23.0982983476938,26.7411562178206,-34.5293581217229));
#25863=CARTESIAN_POINT('Ctrl Pts',(-23.1059391575518,26.7422303004553,-34.5288838814356));
#25864=CARTESIAN_POINT('Ctrl Pts',(-23.1102441025622,26.742826576678,-34.5286164861885));
#25865=CARTESIAN_POINT('Ctrl Pts',(-23.1234908646271,26.7446340783052,-34.5277930566887));
#25866=CARTESIAN_POINT('Ctrl Pts',(-23.1324365157674,26.745816450627,-34.5272361097632));
#25867=CARTESIAN_POINT('Ctrl Pts',(-23.199968826983,26.7544539715437,-34.5230248422883));
#25868=CARTESIAN_POINT('Ctrl Pts',(-23.258742200012,26.7603345431485,-34.519321007381));
#25869=CARTESIAN_POINT('Ctrl Pts',(-23.3243875765316,26.7650850840569,-34.5151371017011));
#25870=CARTESIAN_POINT('Ctrl Pts',(-23.3311356722392,26.7655520696067,-34.5147064640942));
#25871=CARTESIAN_POINT('Ctrl Pts',(-23.3551633488956,26.7671388541319,-34.5131711522595));
#25872=CARTESIAN_POINT('Ctrl Pts',(-23.3724501966957,26.7681406142995,-34.5120629585708));
#25873=CARTESIAN_POINT('Ctrl Pts',(-23.6489381739423,26.7819281614863,-34.4942805394447));
#25874=CARTESIAN_POINT('Ctrl Pts',(-23.9087114015202,26.7634955842362,-34.4766456071947));
#25875=CARTESIAN_POINT('Ctrl Pts',(-24.3227598611288,26.6832538237465,-34.4481740192113));
#25876=CARTESIAN_POINT('Ctrl Pts',(-24.4795746337458,26.6403721360618,-34.4373335505124));
#25877=CARTESIAN_POINT('Ctrl Pts',(-24.6392758716538,26.583435244152,-34.4266578296124));
#25878=CARTESIAN_POINT('Ctrl Pts',(-24.6460366139479,26.580999378516,-34.4262066079734));
#25879=CARTESIAN_POINT('Ctrl Pts',(-24.6563269305794,26.5772528886365,-34.4255209790797));
#25880=CARTESIAN_POINT('Ctrl Pts',(-24.6598623953732,26.5759586786235,-34.4252856256551));
#25881=CARTESIAN_POINT('Ctrl Pts',(-24.665641751141,26.5738315665879,-34.4249012503849));
#25882=CARTESIAN_POINT('Ctrl Pts',(-24.6678869840237,26.5730023596095,-34.4247520108348));
#25883=CARTESIAN_POINT('Ctrl Pts',(-24.6722120584686,26.5713995501179,-34.4244646960888));
#25884=CARTESIAN_POINT('Ctrl Pts',(-24.6742920277781,26.5706262996185,-34.4243265999491));
#25885=CARTESIAN_POINT('Ctrl Pts',(-24.6780981935649,26.5692068411864,-34.4240740376632));
#25886=CARTESIAN_POINT('Ctrl Pts',(-24.6798246278335,26.568561303088,-34.4239595318808));
#25887=CARTESIAN_POINT('Ctrl Pts',(-24.6833279853606,26.5672479215162,-34.4237272806032));
#25888=CARTESIAN_POINT('Ctrl Pts',(-24.6851048654437,26.5665799917916,-34.4236095409975));
#25889=CARTESIAN_POINT('Ctrl Pts',(-24.6902122849053,26.5646549594251,-34.4232712735655));
#25890=CARTESIAN_POINT('Ctrl Pts',(-24.6935413463131,26.5633939027402,-34.4230509840151));
#25891=CARTESIAN_POINT('Ctrl Pts',(-24.7081002806333,26.5578513403004,-34.422088425583));
#25892=CARTESIAN_POINT('Ctrl Pts',(-24.7193084323723,26.5535124796627,-34.4213495674383));
#25893=CARTESIAN_POINT('Ctrl Pts',(-24.9156620868752,26.4762349454548,-34.4084393356143));
#25894=CARTESIAN_POINT('Ctrl Pts',(-25.0937164261527,26.3863522313999,-34.3972459753073));
#25895=CARTESIAN_POINT('Ctrl Pts',(-25.3344371059875,26.2354043869343,-34.3813505390078));
#25896=CARTESIAN_POINT('Ctrl Pts',(-25.4046942725536,26.187372321764,-34.3766105042888));
#25897=CARTESIAN_POINT('Ctrl Pts',(-25.5501366417981,26.0792497867285,-34.3664324978558));
#25898=CARTESIAN_POINT('Ctrl Pts',(-25.6246955804839,26.0184599922566,-34.360988736405));
#25899=CARTESIAN_POINT('Ctrl Pts',(-25.7577443043866,25.8996896161691,-34.3506961002328));
#25900=CARTESIAN_POINT('Ctrl Pts',(-25.8169453570041,25.842626099165,-34.3458797196644));
#25901=CARTESIAN_POINT('Ctrl Pts',(-25.9035930747008,25.752465617683,-34.3384054537156));
#25902=CARTESIAN_POINT('Ctrl Pts',(-25.932668357607,25.7209779289634,-34.3358187005202));
#25903=CARTESIAN_POINT('Ctrl Pts',(-25.9661583935953,25.683225665798,-34.3327405758421));
#25904=CARTESIAN_POINT('Ctrl Pts',(-25.9711904492846,25.6775125350743,-34.3322753719789));
#25905=CARTESIAN_POINT('Ctrl Pts',(-25.9788725227825,25.6687281525263,-34.3315610015756));
#25906=CARTESIAN_POINT('Ctrl Pts',(-25.9815370883529,25.6656696114891,-34.3313124417928));
#25907=CARTESIAN_POINT('Ctrl Pts',(-25.9863871806123,25.660081129468,-34.3308585844646));
#25908=CARTESIAN_POINT('Ctrl Pts',(-25.9885745616518,25.6575527992717,-34.3306533643299));
#25909=CARTESIAN_POINT('Ctrl Pts',(-25.9929656964886,25.6524612234814,-34.3302403148355));
#25910=CARTESIAN_POINT('Ctrl Pts',(-25.9951693593398,25.6498979053328,-34.3300324820844));
#25911=CARTESIAN_POINT('Ctrl Pts',(-26.0014329777226,25.6425887832263,-34.3294401827105));
#25912=CARTESIAN_POINT('Ctrl Pts',(-26.005483159725,25.6378346572087,-34.3290553135174));
#25913=CARTESIAN_POINT('Ctrl Pts',(-26.0226514817313,25.6175633125344,-34.3274158523154));
#25914=CARTESIAN_POINT('Ctrl Pts',(-26.035636304759,25.6019342572194,-34.3261558100426));
#25915=CARTESIAN_POINT('Ctrl Pts',(-26.2795487272023,25.3026378881133,-34.3020968676183));
#25916=CARTESIAN_POINT('Ctrl Pts',(-26.4606222534033,24.9818635050336,-34.2770537867059));
#25917=CARTESIAN_POINT('Ctrl Pts',(-26.6271094795409,24.517415795489,-34.243989226576));
#25918=CARTESIAN_POINT('Ctrl Pts',(-26.6630483763629,24.3946244915293,-34.2355668452985));
#25919=CARTESIAN_POINT('Ctrl Pts',(-26.6933822471434,24.2622334149278,-34.2270389650358));
#25920=CARTESIAN_POINT('Ctrl Pts',(-26.695134826019,24.2544517537131,-34.2265397250902));
#25921=CARTESIAN_POINT('Ctrl Pts',(-26.6974891578114,24.2438141358053,-34.2258600779689));
#25922=CARTESIAN_POINT('Ctrl Pts',(-26.6981159301609,24.2409638347914,-34.2256782457209));
#25923=CARTESIAN_POINT('Ctrl Pts',(-26.6991586035824,24.2361912905079,-34.2253742523619));
#25924=CARTESIAN_POINT('Ctrl Pts',(-26.6995766167567,24.2342695181156,-34.2252519691377));
#25925=CARTESIAN_POINT('Ctrl Pts',(-26.7003967722442,24.2304822487735,-34.2250112344558));
#25926=CARTESIAN_POINT('Ctrl Pts',(-26.7007990167872,24.2286167771921,-34.2248927772435));
#25927=CARTESIAN_POINT('Ctrl Pts',(-26.7016826671531,24.2245009722181,-34.2246316865424));
#25928=CARTESIAN_POINT('Ctrl Pts',(-26.7021633209419,24.2222504743462,-34.2244890966266));
#25929=CARTESIAN_POINT('Ctrl Pts',(-26.7038361053311,24.2143769523061,-34.2239908346009));
#25930=CARTESIAN_POINT('Ctrl Pts',(-26.7050156117136,24.2087512121186,-34.2236358870092));
#25931=CARTESIAN_POINT('Ctrl Pts',(-26.7168820613318,24.1513896106907,-34.2200273371504));
#25932=CARTESIAN_POINT('Ctrl Pts',(-26.7263111805505,24.0993978854145,-34.2168443442268));
#25933=CARTESIAN_POINT('Ctrl Pts',(-26.7351634506009,24.0426760408111,-34.213443655824));
#25934=CARTESIAN_POINT('Ctrl Pts',(-26.7358589654859,24.0381563368825,-34.2131731762908));
#25935=CARTESIAN_POINT('Ctrl Pts',(-26.7375660709119,24.0269036836461,-34.2125009612454));
#25936=CARTESIAN_POINT('Ctrl Pts',(-26.7385659534925,24.0201689537097,-34.212099703183));
#25937=CARTESIAN_POINT('Ctrl Pts',(-26.7616769467061,23.8610344063721,-34.2026424515854));
#25938=CARTESIAN_POINT('Ctrl Pts',(-26.7728598453331,23.7072329408698,-34.1940161951904));
#25939=CARTESIAN_POINT('Ctrl Pts',(-26.773259724431,23.2714384287349,-34.1696554103458));
#25940=CARTESIAN_POINT('Ctrl Pts',(-26.7365681547528,22.9908963587475,-34.1539526948197));
#25941=CARTESIAN_POINT('Ctrl Pts',(-26.6594149078566,22.7020037985452,-34.1358363150405));
#25942=CARTESIAN_POINT('Ctrl Pts',(-26.6548187164703,22.685333240201,-34.1347843480911));
#25943=CARTESIAN_POINT('Ctrl Pts',(-26.6484871384135,22.6630692571995,-34.1333703569692));
#25944=CARTESIAN_POINT('Ctrl Pts',(-26.6468702889653,22.6574421904381,-34.1330122030452));
#25945=CARTESIAN_POINT('Ctrl Pts',(-26.6443176924442,22.6486488246929,-34.1324512916259));
#25946=CARTESIAN_POINT('Ctrl Pts',(-26.6433923923402,22.6454794851254,-34.1322488759086));
#25947=CARTESIAN_POINT('Ctrl Pts',(-26.6416119411351,22.6394157334218,-34.131861122603));
#25948=CARTESIAN_POINT('Ctrl Pts',(-26.6407575907768,22.6365210880454,-34.1316758113937));
#25949=CARTESIAN_POINT('Ctrl Pts',(-26.6387488631193,22.6297503153698,-34.1312418624257));
#25950=CARTESIAN_POINT('Ctrl Pts',(-26.6375912549009,22.6258751588442,-34.1309931190225));
#25951=CARTESIAN_POINT('Ctrl Pts',(-26.6342497521079,22.6147655926262,-34.1302789112706));
#25952=CARTESIAN_POINT('Ctrl Pts',(-26.6320477134568,22.6075367077089,-34.1298128522302));
#25953=CARTESIAN_POINT('Ctrl Pts',(-26.6175229815779,22.5604494765876,-34.1267682854441));
#25954=CARTESIAN_POINT('Ctrl Pts',(-26.6044532094046,22.5208274217603,-34.1241652894908));
#25955=CARTESIAN_POINT('Ctrl Pts',(-26.5634079707793,22.4040658371974,-34.116367397045));
#25956=CARTESIAN_POINT('Ctrl Pts',(-26.5332535193816,22.3277334834705,-34.1111017298354));
#25957=CARTESIAN_POINT('Ctrl Pts',(-26.3824442598128,21.9848864414576,-34.0866719699426));
#25958=CARTESIAN_POINT('Ctrl Pts',(-26.2287880226529,21.7344642084472,-34.0664604335202));
#25959=CARTESIAN_POINT('Ctrl Pts',(-26.0355998160522,21.4985894427246,-34.0462405615771));
#25960=CARTESIAN_POINT('Ctrl Pts',(-26.0276555567921,21.4890036839052,-34.045416869602));
#25961=CARTESIAN_POINT('Ctrl Pts',(-25.9975336278598,21.4530834563791,-34.0423235185648));
#25962=CARTESIAN_POINT('Ctrl Pts',(-25.9749892492306,21.4270580240375,-34.0400684419946));
#25963=CARTESIAN_POINT('Ctrl Pts',(-25.9502649669392,21.3994236470138,-34.0376632217024));
#25964=CARTESIAN_POINT('Ctrl Pts',(-25.9484961347917,21.3974515188744,-34.0374915133806));
#25965=CARTESIAN_POINT('Ctrl Pts',(-25.9433351138718,21.391711584531,-34.036991582895));
#25966=CARTESIAN_POINT('Ctrl Pts',(-25.9399364477877,21.3879495817102,-34.0366637119617));
#25967=CARTESIAN_POINT('Ctrl Pts',(-25.9348891704817,21.3823891560721,-34.0361788075853));
#25968=CARTESIAN_POINT('Ctrl Pts',(-25.9332473879307,21.3805845779198,-34.0360213907168));
#25969=CARTESIAN_POINT('Ctrl Pts',(-25.9287595720053,21.3756629986525,-34.035591949596));
#25970=CARTESIAN_POINT('Ctrl Pts',(-25.9259094512927,21.3725497101926,-34.0353201600074));
#25971=CARTESIAN_POINT('Ctrl Pts',(-25.897736460393,21.3418964777066,-34.032642890099));
#25972=CARTESIAN_POINT('Ctrl Pts',(-25.8719405791128,21.3147923621143,-34.0302656269705));
#25973=CARTESIAN_POINT('Ctrl Pts',(-25.8420088417417,21.2844198170474,-34.0275965287039));
#25974=CARTESIAN_POINT('Ctrl Pts',(-25.8383314087343,21.2807063372392,-34.0272701035406));
#25975=CARTESIAN_POINT('Ctrl Pts',(-25.8329293583653,21.2752778103493,-34.026792812293));
#25976=CARTESIAN_POINT('Ctrl Pts',(-25.8312118308432,21.2735557680694,-34.0266413894239));
#25977=CARTESIAN_POINT('Ctrl Pts',(-25.828160674771,21.2705035099383,-34.0263729720201));
#25978=CARTESIAN_POINT('Ctrl Pts',(-25.8268278288881,21.269172518461,-34.02625591518));
#25979=CARTESIAN_POINT('Ctrl Pts',(-25.824034723487,21.2663881856165,-34.0260110240449));
#25980=CARTESIAN_POINT('Ctrl Pts',(-25.8225742403267,21.264935079012,-34.0258832085064));
#25981=CARTESIAN_POINT('Ctrl Pts',(-25.8187403266074,21.2611278383023,-34.0255482931015));
#25982=CARTESIAN_POINT('Ctrl Pts',(-25.8163646169872,21.2587759870408,-34.0253413754972));
#25983=CARTESIAN_POINT('Ctrl Pts',(-25.8058782996316,21.2484272365452,-34.0244307290252));
#25984=CARTESIAN_POINT('Ctrl Pts',(-25.7977288594532,21.2404695419517,-34.0237300744063));
#25985=CARTESIAN_POINT('Ctrl Pts',(-25.7374045912891,21.1821861744517,-34.0185937615034));
#25986=CARTESIAN_POINT('Ctrl Pts',(-25.6835826396592,21.1335860457188,-34.0142851969908));
#25987=CARTESIAN_POINT('Ctrl Pts',(-25.5664369233721,21.0347726575465,-34.005353924082));
#25988=CARTESIAN_POINT('Ctrl Pts',(-25.5027726338303,20.9850419801022,-34.000754298886));
#25989=CARTESIAN_POINT('Ctrl Pts',(-25.2863692716015,20.8287302467345,-33.9856988285744));
#25990=CARTESIAN_POINT('Ctrl Pts',(-25.12627248535,20.7329938256092,-33.9754464430601));
#25991=CARTESIAN_POINT('Ctrl Pts',(-24.8140903485896,20.5812932963824,-33.9556989004152));
#25992=CARTESIAN_POINT('Ctrl Pts',(-24.6643334649044,20.5219167657888,-33.9463207751583));
#25993=CARTESIAN_POINT('Ctrl Pts',(-24.4999585228515,20.470592697566,-33.9358478357833));
#25994=CARTESIAN_POINT('Ctrl Pts',(-24.489116027262,20.4672699668533,-33.9351562911843));
#25995=CARTESIAN_POINT('Ctrl Pts',(-24.4736504825037,20.4626196327263,-33.9341687730128));
#25996=CARTESIAN_POINT('Ctrl Pts',(-24.4690415624383,20.4612450194121,-33.9338743405505));
#25997=CARTESIAN_POINT('Ctrl Pts',(-24.4611606937386,20.4589137434578,-33.933370640069));
#25998=CARTESIAN_POINT('Ctrl Pts',(-24.4578902630499,20.4579519428427,-33.9331615405289));
#25999=CARTESIAN_POINT('Ctrl Pts',(-24.4515883598676,20.4561094754065,-33.9327584782415));
#26000=CARTESIAN_POINT('Ctrl Pts',(-24.4485571059619,20.4552280698104,-33.9325645399227));
#26001=CARTESIAN_POINT('Ctrl Pts',(-24.4422618004233,20.453407594841,-33.9321616364375));
#26002=CARTESIAN_POINT('Ctrl Pts',(-24.4389975508576,20.4524692292047,-33.9319526485436));
#26003=CARTESIAN_POINT('Ctrl Pts',(-24.4275532764302,20.4491989500023,-33.9312196858708));
#26004=CARTESIAN_POINT('Ctrl Pts',(-24.4193655621167,20.4468942779046,-33.9306948231258));
#26005=CARTESIAN_POINT('Ctrl Pts',(-24.3462253711468,20.4266189789094,-33.9260019181378));
#26006=CARTESIAN_POINT('Ctrl Pts',(-24.2807374823834,20.4106586150428,-33.921768908817));
#26007=CARTESIAN_POINT('Ctrl Pts',(-24.1090165060227,20.3744710932078,-33.9105760508808));
#26008=CARTESIAN_POINT('Ctrl Pts',(-24.0021873925231,20.3575176940976,-33.9035192247818));
#26009=CARTESIAN_POINT('Ctrl Pts',(-23.5723489085688,20.3113095479474,-33.8748149336144));
#26010=CARTESIAN_POINT('Ctrl Pts',(-23.2466207461023,20.3254985094682,-33.8521583126289));
#26011=CARTESIAN_POINT('Ctrl Pts',(-22.9141283549771,20.3908731429603,-33.8307190678589));
#26012=CARTESIAN_POINT('Ctrl Pts',(-22.8997758614409,20.3937968911151,-33.8297974240534));
#26013=CARTESIAN_POINT('Ctrl Pts',(-22.8809036405921,20.3977755451565,-33.828591020595));
#26014=CARTESIAN_POINT('Ctrl Pts',(-22.8763658390729,20.3987424468587,-33.8283013601534));
#26015=CARTESIAN_POINT('Ctrl Pts',(-22.8695099129511,20.4002187727558,-33.8278643756535));
#26016=CARTESIAN_POINT('Ctrl Pts',(-22.8671902618453,20.4007209584248,-33.8277166375054));
#26017=CARTESIAN_POINT('Ctrl Pts',(-22.8630426885942,20.4016236720595,-33.8274526828081));
#26018=CARTESIAN_POINT('Ctrl Pts',(-22.8612145629831,20.4020232290674,-33.827336410379));
#26019=CARTESIAN_POINT('Ctrl Pts',(-22.8573209593397,20.4028777729977,-33.8270889210192));
#26020=CARTESIAN_POINT('Ctrl Pts',(-22.8552555864449,20.403333199744,-33.8269577302005));
#26021=CARTESIAN_POINT('Ctrl Pts',(-22.849688166731,20.4045665965518,-33.8266043328559));
#26022=CARTESIAN_POINT('Ctrl Pts',(-22.846186955032,20.4053483843368,-33.8263823469187));
#26023=CARTESIAN_POINT('Ctrl Pts',(-22.8291260887385,20.4091878350311,-33.8253018637408));
#26024=CARTESIAN_POINT('Ctrl Pts',(-22.8155847381095,20.4123274170791,-33.8244480345528));
#26025=CARTESIAN_POINT('Ctrl Pts',(-22.702288799366,20.4393688551679,-33.817332637962));
#26026=CARTESIAN_POINT('Ctrl Pts',(-22.6036961517975,20.4679359609417,-33.8113243182266));
#26027=CARTESIAN_POINT('Ctrl Pts',(-22.1430373343921,20.6256080320322,-33.7834093715236));
#26028=CARTESIAN_POINT('Ctrl Pts',(-21.8046557563379,20.8140647491773,-33.7629530372165));
#26029=CARTESIAN_POINT('Ctrl Pts',(-21.4920140997596,21.0702993370409,-33.7385002728303));
#26030=CARTESIAN_POINT('Ctrl Pts',(-21.4767457391084,21.0830511122999,-33.7372912672248));
#26031=CARTESIAN_POINT('Ctrl Pts',(-21.4569742189052,21.0998769871235,-33.7357058089206));
#26032=CARTESIAN_POINT('Ctrl Pts',(-21.4523629121682,21.1038237982725,-33.7353346041626));
#26033=CARTESIAN_POINT('Ctrl Pts',(-21.4449592670849,21.1101968937309,-33.7347363022266));
#26034=CARTESIAN_POINT('Ctrl Pts',(-21.4421598930686,21.1126150128746,-33.7345095436871));
#26035=CARTESIAN_POINT('Ctrl Pts',(-21.4368660551116,21.1172038068843,-33.7340797054491));
#26036=CARTESIAN_POINT('Ctrl Pts',(-21.4343707547595,21.1193735131893,-33.733876666203));
#26037=CARTESIAN_POINT('Ctrl Pts',(-21.4294505454255,21.1236650348486,-33.7334754611075));
#26038=CARTESIAN_POINT('Ctrl Pts',(-21.4270254701923,21.1257866544351,-33.733277303564));
#26039=CARTESIAN_POINT('Ctrl Pts',(-21.4195096468657,21.1323819291521,-33.7326618897988));
#26040=CARTESIAN_POINT('Ctrl Pts',(-21.4144298500582,21.1368679864196,-33.7322441145748));
#26041=CARTESIAN_POINT('Ctrl Pts',(-21.3876270925961,21.1606888694077,-33.7300300358509));
#26042=CARTESIAN_POINT('Ctrl Pts',(-21.3661530007074,21.1803005416068,-33.7282220846225));
#26043=CARTESIAN_POINT('Ctrl Pts',(-21.3070410851465,21.2357715425962,-33.7231476532436));
#26044=CARTESIAN_POINT('Ctrl Pts',(-21.2700024810063,21.2722536194351,-33.7198545779762));
#26045=CARTESIAN_POINT('Ctrl Pts',(-21.1817407988725,21.3634991863666,-33.7117201275055));
#26046=CARTESIAN_POINT('Ctrl Pts',(-21.1315171952111,21.4191833107751,-33.7068402480703));
#26047=CARTESIAN_POINT('Ctrl Pts',(-20.974648270876,21.6058028850584,-33.690764910758));
#26048=CARTESIAN_POINT('Ctrl Pts',(-20.8763439000876,21.7433695455611,-33.6793212401047));
#26049=CARTESIAN_POINT('Ctrl Pts',(-20.6945525037141,22.0453205366658,-33.6554792276729));
#26050=CARTESIAN_POINT('Ctrl Pts',(-20.6134386447165,22.2104820855729,-33.6431294467934));
#26051=CARTESIAN_POINT('Ctrl Pts',(-20.5429793028093,22.3915730568911,-33.6308941634161));
#26052=CARTESIAN_POINT('Ctrl Pts',(-20.539176480956,22.401491711204,-33.6302280575105));
#26053=CARTESIAN_POINT('Ctrl Pts',(-20.5342245208832,22.4146011337601,-33.6293531628402));
#26054=CARTESIAN_POINT('Ctrl Pts',(-20.5330313345554,22.417775023125,-33.6291417677605));
#26055=CARTESIAN_POINT('Ctrl Pts',(-20.5311899254078,22.4226967606199,-33.6288146207904));
#26056=CARTESIAN_POINT('Ctrl Pts',(-20.5305382108163,22.4244432859128,-33.628698658716));
#26057=CARTESIAN_POINT('Ctrl Pts',(-20.5292427416423,22.4279242225583,-33.6284677975111));
#26058=CARTESIAN_POINT('Ctrl Pts',(-20.5285989692078,22.4296586117499,-33.6283528981228));
#26059=CARTESIAN_POINT('Ctrl Pts',(-20.5271488963663,22.4335755925932,-33.6280936950383));
#26060=CARTESIAN_POINT('Ctrl Pts',(-20.5263434675872,22.4357584992534,-33.6279494444835));
#26061=CARTESIAN_POINT('Ctrl Pts',(-20.5239641549762,22.4422285787449,-33.6275224810836));
#26062=CARTESIAN_POINT('Ctrl Pts',(-20.5223970108164,22.4465182499633,-33.6272401726775));
#26063=CARTESIAN_POINT('Ctrl Pts',(-20.5100282925595,22.4805991636035,-33.6250032573602));
#26064=CARTESIAN_POINT('Ctrl Pts',(-20.4996570483137,22.5105462591293,-33.6230739679818));
#26065=CARTESIAN_POINT('Ctrl Pts',(-20.4600280880389,22.6306772103861,-33.6154606117935));
#26066=CARTESIAN_POINT('Ctrl Pts',(-20.4343120097873,22.7219869591672,-33.6099540842873));
#26067=CARTESIAN_POINT('Ctrl Pts',(-20.3454608025972,23.1007901843353,-33.5877542339657));
#26068=CARTESIAN_POINT('Ctrl Pts',(-20.3178151731128,23.3951199466005,-33.5718637579957));
#26069=CARTESIAN_POINT('Ctrl Pts',(-20.3344206511219,23.7801174801264,-33.5493579025877));
#26070=CARTESIAN_POINT('Ctrl Pts',(-20.3422003858697,23.8708950177142,-33.5439386155613));
#26071=CARTESIAN_POINT('Ctrl Pts',(-20.3550843030089,23.9711052124267,-33.5377879411271));
#26072=CARTESIAN_POINT('Ctrl Pts',(-20.3564017116921,23.9809890225315,-33.5371794886299));
#26073=CARTESIAN_POINT('Ctrl Pts',(-20.3583871955912,23.9953749329228,-33.5362912002658));
#26074=CARTESIAN_POINT('Ctrl Pts',(-20.359018981669,23.9998820511298,-33.5360125145795));
#26075=CARTESIAN_POINT('Ctrl Pts',(-20.3601332891304,24.0077107774697,-33.535527772931));
#26076=CARTESIAN_POINT('Ctrl Pts',(-20.3606114574496,24.0110330062804,-33.5353218552954));
#26077=CARTESIAN_POINT('Ctrl Pts',(-20.3615468750801,24.017460892261,-33.5349230331689));
#26078=CARTESIAN_POINT('Ctrl Pts',(-20.3620034738697,24.0205666414935,-33.5347301495402));
#26079=CARTESIAN_POINT('Ctrl Pts',(-20.3629742052434,24.0271031019756,-33.5343238077794));
#26080=CARTESIAN_POINT('Ctrl Pts',(-20.3634893406181,24.0305336582159,-33.5341103180113));
#26081=CARTESIAN_POINT('Ctrl Pts',(-20.3653902792497,24.0430552952626,-33.5333302371743));
#26082=CARTESIAN_POINT('Ctrl Pts',(-20.3668094438403,24.052141199039,-33.5327625870518));
#26083=CARTESIAN_POINT('Ctrl Pts',(-20.3844673139956,24.1621031661328,-33.5258728293296));
#26084=CARTESIAN_POINT('Ctrl Pts',(-20.4054538206304,24.262147530655,-33.5193997821666));
#26085=CARTESIAN_POINT('Ctrl Pts',(-20.4406702743354,24.3976288743335,-33.510336315347));
#26086=CARTESIAN_POINT('Ctrl Pts',(-20.4508302979962,24.4340681947827,-33.5078688015035));
#26087=CARTESIAN_POINT('Ctrl Pts',(-20.5416273151462,24.7388698104988,-33.4869829225475));
#26088=CARTESIAN_POINT('Ctrl Pts',(-20.6562932973689,24.9958000372653,-33.4676183517231));
#26089=CARTESIAN_POINT('Ctrl Pts',(-20.8498139941704,25.3114644951791,-33.4431268721492));
#26090=CARTESIAN_POINT('Ctrl Pts',(-20.9001124645207,25.3862800472435,-33.4372766156257));
#26091=CARTESIAN_POINT('Ctrl Pts',(-20.957285261597,25.4640653366161,-33.4312247337822));
#26092=CARTESIAN_POINT('Ctrl Pts',(-20.9611000124356,25.4692230759633,-33.4308236024124));
#26093=CARTESIAN_POINT('Ctrl Pts',(-20.9664097146433,25.4763574095024,-33.4302689986703));
#26094=CARTESIAN_POINT('Ctrl Pts',(-20.9678915503622,25.4783436772932,-33.4301146188623));
#26095=CARTESIAN_POINT('Ctrl Pts',(-20.9704417728123,25.4817538078126,-33.4298496211275));
#26096=CARTESIAN_POINT('Ctrl Pts',(-20.9715090479577,25.4831784941697,-33.4297389251703));
#26097=CARTESIAN_POINT('Ctrl Pts',(-20.973715424886,25.4861186670378,-33.4295105104022));
#26098=CARTESIAN_POINT('Ctrl Pts',(-20.9748546813497,25.4876340297954,-33.4293928035086));
#26099=CARTESIAN_POINT('Ctrl Pts',(-20.9775313935578,25.4911878801958,-33.4291167956924));
#26100=CARTESIAN_POINT('Ctrl Pts',(-20.9790699398956,25.4932255529728,-33.4289585718772));
#26101=CARTESIAN_POINT('Ctrl Pts',(-20.9840695703234,25.4998307970993,-33.4284457720489));
#26102=CARTESIAN_POINT('Ctrl Pts',(-20.9875404415114,25.5043909986914,-33.4280918835224));
#26103=CARTESIAN_POINT('Ctrl Pts',(-21.0825663294083,25.6285520875382,-33.4184597173937));
#26104=CARTESIAN_POINT('Ctrl Pts',(-21.1823965282736,25.7416164691065,-33.4097663298791));
#26105=CARTESIAN_POINT('Ctrl Pts',(-21.5214864338104,26.0753070640255,-33.3828610859152));
#26106=CARTESIAN_POINT('Ctrl Pts',(-21.7862386107151,26.2668469218924,-33.365236529596));
#26107=CARTESIAN_POINT('Ctrl Pts',(-22.0750360407425,26.4155367876319,-33.3457833635692));
#26108=CARTESIAN_POINT('Origin',(-23.5502525316942,23.5502525316942,-77.3107734492734));
#26109=CARTESIAN_POINT('',(-22.0750360153402,26.4155367745532,-31.8492183260801));
#26110=CARTESIAN_POINT('',(-22.0750360188393,26.4155367763548,-32.0936416103654));
#26111=CARTESIAN_POINT('',(-22.0750360153461,26.4155367745563,-77.3107734492734));
#26112=CARTESIAN_POINT('Ctrl Pts',(-22.0750360153402,26.4155367745532,-31.8492183260801));
#26113=CARTESIAN_POINT('Ctrl Pts',(-22.0738944921894,26.4149490514294,-31.8493005742725));
#26114=CARTESIAN_POINT('Ctrl Pts',(-22.0727533154471,26.414360643657,-31.8493827878888));
#26115=CARTESIAN_POINT('Ctrl Pts',(-22.0672699001479,26.411529163442,-31.8497777814017));
#26116=CARTESIAN_POINT('Ctrl Pts',(-22.0629323917442,26.4092768846506,-31.8500900877478));
#26117=CARTESIAN_POINT('Ctrl Pts',(-22.042973497031,26.398855388619,-31.8515264395472));
#26118=CARTESIAN_POINT('Ctrl Pts',(-22.0274138030302,26.3905677542308,-31.8526441799446));
#26119=CARTESIAN_POINT('Ctrl Pts',(-22.005523084465,26.3786763921286,-31.8542130139914));
#26120=CARTESIAN_POINT('Ctrl Pts',(-21.9991353961047,26.3751784127566,-31.8546703492278));
#26121=CARTESIAN_POINT('Ctrl Pts',(-21.9879855904546,26.369023416774,-31.8554677748243));
#26122=CARTESIAN_POINT('Ctrl Pts',(-21.9832182875004,26.3663759268647,-31.8558084524994));
#26123=CARTESIAN_POINT('Ctrl Pts',(-21.9762821996464,26.3625009499911,-31.8563036855365));
#26124=CARTESIAN_POINT('Ctrl Pts',(-21.9741081150861,26.3612830456652,-31.8564588524827));
#26125=CARTESIAN_POINT('Ctrl Pts',(-21.9703858958006,26.3591922131341,-31.8567244031774));
#26126=CARTESIAN_POINT('Ctrl Pts',(-21.9688370690047,26.3583205251025,-31.8568348673953));
#26127=CARTESIAN_POINT('Ctrl Pts',(-21.9657550741822,26.3565826032586,-31.857054613735));
#26128=CARTESIAN_POINT('Ctrl Pts',(-21.9642218972916,26.3557163953365,-31.8571638972305));
#26129=CARTESIAN_POINT('Ctrl Pts',(-21.9605961698484,26.353664024762,-31.8574222618296));
#26130=CARTESIAN_POINT('Ctrl Pts',(-21.9585042322179,26.3524767731539,-31.8575712721461));
#26131=CARTESIAN_POINT('Ctrl Pts',(-21.9522826605605,26.3489365873753,-31.8580142714327));
#26132=CARTESIAN_POINT('Ctrl Pts',(-21.9481568771009,26.3465768452873,-31.8583078221464));
#26133=CARTESIAN_POINT('Ctrl Pts',(-21.9104392548507,26.3248933723161,-31.8609895620944));
#26134=CARTESIAN_POINT('Ctrl Pts',(-21.8771914845096,26.3049732866924,-31.8633398248362));
#26135=CARTESIAN_POINT('Ctrl Pts',(-21.6094054099348,26.1378944182269,-31.8822251423793));
#26136=CARTESIAN_POINT('Ctrl Pts',(-21.3943349555691,25.961651090485,-31.8971909469708));
#26137=CARTESIAN_POINT('Ctrl Pts',(-21.1781705267215,25.7321807832313,-31.914974747874));
#26138=CARTESIAN_POINT('Ctrl Pts',(-21.1524126513311,25.7038420339421,-31.9171442098866));
#26139=CARTESIAN_POINT('Ctrl Pts',(-21.0635867614361,25.6025464314741,-31.9248238993856));
#26140=CARTESIAN_POINT('Ctrl Pts',(-21.0032981092715,25.5272294637784,-31.9304028332972));
#26141=CARTESIAN_POINT('Ctrl Pts',(-20.909347088567,25.3984156320949,-31.939839795394));
#26142=CARTESIAN_POINT('Ctrl Pts',(-20.8737177100792,25.3464287252652,-31.9436217478048));
#26143=CARTESIAN_POINT('Ctrl Pts',(-20.835103380396,25.2863841205163,-31.9479734280845));
#26144=CARTESIAN_POINT('Ctrl Pts',(-20.830597536065,25.2793171661598,-31.9484853402299));
#26145=CARTESIAN_POINT('Ctrl Pts',(-20.8238661677569,25.2686682960818,-31.949256359588));
#26146=CARTESIAN_POINT('Ctrl Pts',(-20.8216199990823,25.2650994188721,-31.9495146999878));
#26147=CARTESIAN_POINT('Ctrl Pts',(-20.8177672124186,25.2589510941145,-31.9499596598908));
#26148=CARTESIAN_POINT('Ctrl Pts',(-20.8161572224185,25.2563737574476,-31.9501461542553));
#26149=CARTESIAN_POINT('Ctrl Pts',(-20.8128474380097,25.2510586054515,-31.9505306954989));
#26150=CARTESIAN_POINT('Ctrl Pts',(-20.8111481002759,25.2483205106389,-31.950728758998));
#26151=CARTESIAN_POINT('Ctrl Pts',(-20.8070643168476,25.2417183448566,-31.9512062591381));
#26152=CARTESIAN_POINT('Ctrl Pts',(-20.8046839295779,25.2378517820837,-31.9514858450529));
#26153=CARTESIAN_POINT('Ctrl Pts',(-20.7973950915188,25.2259559775145,-31.9523458317469));
#26154=CARTESIAN_POINT('Ctrl Pts',(-20.792513665359,25.2179103102419,-31.9529272242997));
#26155=CARTESIAN_POINT('Ctrl Pts',(-20.735423768802,25.1228774396715,-31.9597917212386));
#26156=CARTESIAN_POINT('Ctrl Pts',(-20.6873209365657,25.033502008427,-31.9662235328316));
#26157=CARTESIAN_POINT('Ctrl Pts',(-20.5185056972325,24.6809264254587,-31.9915452865556));
#26158=CARTESIAN_POINT('Ctrl Pts',(-20.4292535129324,24.4042015975014,-32.0114653686875));
#26159=CARTESIAN_POINT('Ctrl Pts',(-20.362656743404,24.0330031812092,-32.0366528381726));
#26160=CARTESIAN_POINT('Ctrl Pts',(-20.350694977246,23.9460418892281,-32.0424342360964));
#26161=CARTESIAN_POINT('Ctrl Pts',(-20.3402134011377,23.8370278803283,-32.0494509881381));
#26162=CARTESIAN_POINT('Ctrl Pts',(-20.3383497153814,23.8153405885105,-32.0508355272982));
#26163=CARTESIAN_POINT('Ctrl Pts',(-20.3360633767315,23.785152533171,-32.0527454214404));
#26164=CARTESIAN_POINT('Ctrl Pts',(-20.3354544953238,23.77666702709,-32.0532803668208));
#26165=CARTESIAN_POINT('Ctrl Pts',(-20.3345913191728,23.7639313904858,-32.0540802945212));
#26166=CARTESIAN_POINT('Ctrl Pts',(-20.334311840174,23.7596830870683,-32.0543466380783));
#26167=CARTESIAN_POINT('Ctrl Pts',(-20.3338752870159,23.7528401399555,-32.0547748427269));
#26168=CARTESIAN_POINT('Ctrl Pts',(-20.333712933087,23.7502458561104,-32.0549369958535));
#26169=CARTESIAN_POINT('Ctrl Pts',(-20.3334086408069,23.7452872827178,-32.0552465656321));
#26170=CARTESIAN_POINT('Ctrl Pts',(-20.3332661699112,23.7429230292651,-32.0553940120786));
#26171=CARTESIAN_POINT('Ctrl Pts',(-20.3330175817601,23.7387206440339,-32.055655812217));
#26172=CARTESIAN_POINT('Ctrl Pts',(-20.3329104333136,23.7368825788505,-32.0557702242812));
#26173=CARTESIAN_POINT('Ctrl Pts',(-20.3327006061954,23.733229237687,-32.0559974389361));
#26174=CARTESIAN_POINT('Ctrl Pts',(-20.3325978888635,23.7314139727516,-32.0561102434532));
#26175=CARTESIAN_POINT('Ctrl Pts',(-20.3323207209375,23.7264411365231,-32.056419012715));
#26176=CARTESIAN_POINT('Ctrl Pts',(-20.3321493811051,23.7232833830596,-32.0566148012797));
#26177=CARTESIAN_POINT('Ctrl Pts',(-20.3315113630982,23.7111960230365,-32.0573631931802));
#26178=CARTESIAN_POINT('Ctrl Pts',(-20.3310771957264,23.7022646318452,-32.0579139801095));
#26179=CARTESIAN_POINT('Ctrl Pts',(-20.3243945682708,23.5518916312754,-32.0671519488671));
#26180=CARTESIAN_POINT('Ctrl Pts',(-20.3274353481881,23.4101702750807,-32.075334800481));
#26181=CARTESIAN_POINT('Ctrl Pts',(-20.3494043449505,23.1593159930794,-32.0895950084584));
#26182=CARTESIAN_POINT('Ctrl Pts',(-20.3646422121306,23.0501040211017,-32.0957271416361));
#26183=CARTESIAN_POINT('Ctrl Pts',(-20.4130198373575,22.7984372168493,-32.1100571274531));
#26184=CARTESIAN_POINT('Ctrl Pts',(-20.4503141307594,22.6570376743474,-32.1182659413323));
#26185=CARTESIAN_POINT('Ctrl Pts',(-20.5282390690473,22.4264039314636,-32.1323903339225));
#26186=CARTESIAN_POINT('Ctrl Pts',(-20.5635739952306,22.3356128585726,-32.1381485448151));
#26187=CARTESIAN_POINT('Ctrl Pts',(-20.6100416882379,22.2305616441219,-32.1451086628262));
#26188=CARTESIAN_POINT('Ctrl Pts',(-20.6172513823092,22.2146148257375,-32.1461734460391));
#26189=CARTESIAN_POINT('Ctrl Pts',(-20.6269659676147,22.1935855452764,-32.1475887946829));
#26190=CARTESIAN_POINT('Ctrl Pts',(-20.6293549820729,22.1884496268168,-32.1479353509995));
#26191=CARTESIAN_POINT('Ctrl Pts',(-20.6332954911716,22.1800363683645,-32.1485045238402));
#26192=CARTESIAN_POINT('Ctrl Pts',(-20.6348390057779,22.1767552862517,-32.1487268633484));
#26193=CARTESIAN_POINT('Ctrl Pts',(-20.6378376489551,22.1704088350346,-32.1491576408878));
#26194=CARTESIAN_POINT('Ctrl Pts',(-20.639292088475,22.1673431441044,-32.1493660547535));
#26195=CARTESIAN_POINT('Ctrl Pts',(-20.6426568797261,22.1602796113165,-32.1498470035502));
#26196=CARTESIAN_POINT('Ctrl Pts',(-20.6445706366749,22.156283407441,-32.1501196567699));
#26197=CARTESIAN_POINT('Ctrl Pts',(-20.6505519696393,22.1438593480508,-32.1509690655069));
#26198=CARTESIAN_POINT('Ctrl Pts',(-20.6546479901376,22.1354453107157,-32.1515468126199));
#26199=CARTESIAN_POINT('Ctrl Pts',(-20.6897042913362,22.06422265597,-32.1564587019866));
#26200=CARTESIAN_POINT('Ctrl Pts',(-20.7226653006145,22.0024249459316,-32.1608628475315));
#26201=CARTESIAN_POINT('Ctrl Pts',(-20.7618678909811,21.9343622476178,-32.1658815178235));
#26202=CARTESIAN_POINT('Ctrl Pts',(-20.7661543193358,21.926988087279,-32.1664275136878));
#26203=CARTESIAN_POINT('Ctrl Pts',(-20.7971646554925,21.8741235841165,-32.1703579458718));
#26204=CARTESIAN_POINT('Ctrl Pts',(-20.8249715891385,21.829280597049,-32.1737789202992));
#26205=CARTESIAN_POINT('Ctrl Pts',(-20.9631020303543,21.6182721797139,-32.1902929045161));
#26206=CARTESIAN_POINT('Ctrl Pts',(-21.0875844071843,21.4619167346764,-32.2038320553028));
#26207=CARTESIAN_POINT('Ctrl Pts',(-21.3459930509058,21.1928129195055,-32.2290492470429));
#26208=CARTESIAN_POINT('Ctrl Pts',(-21.4762336897309,21.0774518288264,-32.2406900247347));
#26209=CARTESIAN_POINT('Ctrl Pts',(-21.6207619097685,20.9689287081519,-32.2520673428584));
#26210=CARTESIAN_POINT('Ctrl Pts',(-21.6263835880648,20.9647361360828,-32.2525075988885));
#26211=CARTESIAN_POINT('Ctrl Pts',(-21.6349911982024,20.9583603140136,-32.2531781564823));
#26212=CARTESIAN_POINT('Ctrl Pts',(-21.6379672339975,20.9561638315572,-32.253409355333));
#26213=CARTESIAN_POINT('Ctrl Pts',(-21.6428528656709,20.9525709359393,-32.2537878428392));
#26214=CARTESIAN_POINT('Ctrl Pts',(-21.6447602191429,20.9511715006826,-32.2539353400084));
#26215=CARTESIAN_POINT('Ctrl Pts',(-21.6483608226076,20.9485358129148,-32.2542132761647));
#26216=CARTESIAN_POINT('Ctrl Pts',(-21.6500537397969,20.947299111212,-32.2543437464643));
#26217=CARTESIAN_POINT('Ctrl Pts',(-21.6532258410472,20.9449865869545,-32.2545878228032));
#26218=CARTESIAN_POINT('Ctrl Pts',(-21.654704730162,20.9439103745695,-32.2547014559994));
#26219=CARTESIAN_POINT('Ctrl Pts',(-21.6577038084725,20.9417317978579,-32.2549315725779));
#26220=CARTESIAN_POINT('Ctrl Pts',(-21.659224039156,20.9406295073716,-32.2550480507664));
#26221=CARTESIAN_POINT('Ctrl Pts',(-21.663547097536,20.9375007008111,-32.2553788044352));
#26222=CARTESIAN_POINT('Ctrl Pts',(-21.6663522362212,20.9354773593231,-32.2555928581835));
#26223=CARTESIAN_POINT('Ctrl Pts',(-21.6782275153922,20.9269407716948,-32.2564966720176));
#26224=CARTESIAN_POINT('Ctrl Pts',(-21.6873283589735,20.9204700716531,-32.257183512027));
#26225=CARTESIAN_POINT('Ctrl Pts',(-21.8417568821177,20.8118753613712,-32.2687436664392));
#26226=CARTESIAN_POINT('Ctrl Pts',(-21.9952732946475,20.7218738024144,-32.2788334421321));
#26227=CARTESIAN_POINT('Ctrl Pts',(-22.3343548446947,20.5590828974625,-32.2999369969224));
#26228=CARTESIAN_POINT('Ctrl Pts',(-22.5208049917386,20.4899032728678,-32.3108918663511));
#26229=CARTESIAN_POINT('Ctrl Pts',(-22.8226886985239,20.4086277445212,-32.328898755521));
#26230=CARTESIAN_POINT('Ctrl Pts',(-22.9344347631091,20.3848268816883,-32.3356126739721));
#26231=CARTESIAN_POINT('Ctrl Pts',(-23.0662960922209,20.3639886529421,-32.3436927811906));
#26232=CARTESIAN_POINT('Ctrl Pts',(-23.08541887836,20.361142782923,-32.3448682847374));
#26233=CARTESIAN_POINT('Ctrl Pts',(-23.1103889015759,20.3576560775315,-32.3464084159436));
#26234=CARTESIAN_POINT('Ctrl Pts',(-23.1162141924825,20.3568589055336,-32.3467680825904));
#26235=CARTESIAN_POINT('Ctrl Pts',(-23.1256829326285,20.3555895266754,-32.3473533118936));
#26236=CARTESIAN_POINT('Ctrl Pts',(-23.129325083379,20.3551075986491,-32.3475785663422));
#26237=CARTESIAN_POINT('Ctrl Pts',(-23.1363161862689,20.3541946996649,-32.3480112251396));
#26238=CARTESIAN_POINT('Ctrl Pts',(-23.1396650090683,20.3537627616706,-32.3482185985687));
#26239=CARTESIAN_POINT('Ctrl Pts',(-23.1473033010481,20.3527897606273,-32.3486918811889));
#26240=CARTESIAN_POINT('Ctrl Pts',(-23.1515931859479,20.352252065685,-32.3489578965885));
#26241=CARTESIAN_POINT('Ctrl Pts',(-23.1649636418193,20.3506035314565,-32.3497876474889));
#26242=CARTESIAN_POINT('Ctrl Pts',(-23.1740478098553,20.3495227308705,-32.3503523316397));
#26243=CARTESIAN_POINT('Ctrl Pts',(-23.2446340338875,20.3414292927383,-32.3547474831137));
#26244=CARTESIAN_POINT('Ctrl Pts',(-23.3063183171339,20.3361516489869,-32.3586324261187));
#26245=CARTESIAN_POINT('Ctrl Pts',(-23.3731385183356,20.3323691395817,-32.3628926225131));
#26246=CARTESIAN_POINT('Ctrl Pts',(-23.3781646436171,20.3320964358403,-32.3632133823488));
#26247=CARTESIAN_POINT('Ctrl Pts',(-23.4057085146813,20.330666692207,-32.3649729135784));
#26248=CARTESIAN_POINT('Ctrl Pts',(-23.4282368536426,20.3297342372304,-32.3664183604982));
#26249=CARTESIAN_POINT('Ctrl Pts',(-23.7063524398426,20.3211452726332,-32.3843406913961));
#26250=CARTESIAN_POINT('Ctrl Pts',(-23.9619326367737,20.3436996992466,-32.4017322505713));
#26251=CARTESIAN_POINT('Ctrl Pts',(-24.2472883519581,20.4035795680835,-32.421408368598));
#26252=CARTESIAN_POINT('Ctrl Pts',(-24.282342709261,20.4115499767024,-32.4238280008759));
#26253=CARTESIAN_POINT('Ctrl Pts',(-24.4418859928224,20.4506441107599,-32.4348345355536));
#26254=CARTESIAN_POINT('Ctrl Pts',(-24.5645973727856,20.4886033338312,-32.4432871457373));
#26255=CARTESIAN_POINT('Ctrl Pts',(-24.6892746159681,20.5354938664154,-32.4516433691759));
#26256=CARTESIAN_POINT('Ctrl Pts',(-24.6938135609635,20.5372126561868,-32.4519472507496));
#26257=CARTESIAN_POINT('Ctrl Pts',(-24.7010072225706,20.539955320554,-32.4524283191608));
#26258=CARTESIAN_POINT('Ctrl Pts',(-24.7036644732938,20.5409724598006,-32.4526059015662));
#26259=CARTESIAN_POINT('Ctrl Pts',(-24.7086943357708,20.5429054255215,-32.4529418150293));
#26260=CARTESIAN_POINT('Ctrl Pts',(-24.7110672149856,20.5438205431735,-32.4531001882837));
#26261=CARTESIAN_POINT('Ctrl Pts',(-24.7151824372747,20.5454132061463,-32.4533746798818));
#26262=CARTESIAN_POINT('Ctrl Pts',(-24.7169252763667,20.5460894595254,-32.4534908766082));
#26263=CARTESIAN_POINT('Ctrl Pts',(-24.7203095556865,20.547406010912,-32.4537164048956));
#26264=CARTESIAN_POINT('Ctrl Pts',(-24.721951056291,20.5480461373464,-32.4538257466579));
#26265=CARTESIAN_POINT('Ctrl Pts',(-24.7258357204919,20.549564688532,-32.4540843961509));
#26266=CARTESIAN_POINT('Ctrl Pts',(-24.7280784295514,20.5504442844373,-32.4542336327187));
#26267=CARTESIAN_POINT('Ctrl Pts',(-24.7347563757129,20.5530720344145,-32.4546777471464));
#26268=CARTESIAN_POINT('Ctrl Pts',(-24.7391887474357,20.5548275258967,-32.4549721836515));
#26269=CARTESIAN_POINT('Ctrl Pts',(-24.7800003394468,20.5710962801882,-32.4576802801949));
#26270=CARTESIAN_POINT('Ctrl Pts',(-24.8161180324508,20.5862625664614,-32.4600551922295));
#26271=CARTESIAN_POINT('Ctrl Pts',(-24.9395728826377,20.6407713765239,-32.468127346537));
#26272=CARTESIAN_POINT('Ctrl Pts',(-25.0254332322613,20.6833488495696,-32.4736622282515));
#26273=CARTESIAN_POINT('Ctrl Pts',(-25.1628325562598,20.7592942998411,-32.4825877250237));
#26274=CARTESIAN_POINT('Ctrl Pts',(-25.2155364877084,20.790417048588,-32.486028669322));
#26275=CARTESIAN_POINT('Ctrl Pts',(-25.350890996741,20.8756365801258,-32.4949885575412));
#26276=CARTESIAN_POINT('Ctrl Pts',(-25.431995712337,20.9320638626509,-32.5004831381294));
#26277=CARTESIAN_POINT('Ctrl Pts',(-25.6068369566286,21.0660335188971,-32.5128574011248));
#26278=CARTESIAN_POINT('Ctrl Pts',(-25.6990292764379,21.1453328370731,-32.5197562740335));
#26279=CARTESIAN_POINT('Ctrl Pts',(-25.832996411724,21.2744309134998,-32.5306092668335));
#26280=CARTESIAN_POINT('Ctrl Pts',(-25.8781150764888,21.3206026033689,-32.5344242374469));
#26281=CARTESIAN_POINT('Ctrl Pts',(-25.9449690559482,21.3932593340023,-32.5403519247257));
#26282=CARTESIAN_POINT('Ctrl Pts',(-25.9677204057971,21.4187892254526,-32.5424211957393));
#26283=CARTESIAN_POINT('Ctrl Pts',(-25.9947195720186,21.4500741340144,-32.5449427360589));
#26284=CARTESIAN_POINT('Ctrl Pts',(-25.9993606192261,21.4554881087556,-32.5453785932236));
#26285=CARTESIAN_POINT('Ctrl Pts',(-26.0065458234289,21.4639264673529,-32.5460571678793));
#26286=CARTESIAN_POINT('Ctrl Pts',(-26.0091024701993,21.4669402263825,-32.5462993702967));
#26287=CARTESIAN_POINT('Ctrl Pts',(-26.0135969057829,21.4722580367943,-32.5467264779922));
#26288=CARTESIAN_POINT('Ctrl Pts',(-26.0155370255143,21.4745601193603,-32.5469112872427));
#26289=CARTESIAN_POINT('Ctrl Pts',(-26.0196331029982,21.4794342344749,-32.5473023975595));
#26290=CARTESIAN_POINT('Ctrl Pts',(-26.0217882732762,21.4820069215261,-32.5475087305625));
#26291=CARTESIAN_POINT('Ctrl Pts',(-26.0278658715866,21.4892849854746,-32.548092147139));
#26292=CARTESIAN_POINT('Ctrl Pts',(-26.0317788922787,21.4939981676919,-32.5484696140535));
#26293=CARTESIAN_POINT('Ctrl Pts',(-26.0479959472624,21.5136451077219,-32.5500416793535));
#26294=CARTESIAN_POINT('Ctrl Pts',(-26.0601785977775,21.5286781239875,-32.5512411894322));
#26295=CARTESIAN_POINT('Ctrl Pts',(-26.3158295101706,21.8500168329163,-32.5768142654837));
#26296=CARTESIAN_POINT('Ctrl Pts',(-26.5015927998284,22.1979864031684,-32.6038166739562));
#26297=CARTESIAN_POINT('Ctrl Pts',(-26.6499297077645,22.66283580488,-32.6362805901247));
#26298=CARTESIAN_POINT('Ctrl Pts',(-26.6752124291342,22.7564410164609,-32.6426185368125));
#26299=CARTESIAN_POINT('Ctrl Pts',(-26.6981695169157,22.8597343840643,-32.6492974718204));
#26300=CARTESIAN_POINT('Ctrl Pts',(-26.7000631243058,22.8684241859521,-32.6498569400747));
#26301=CARTESIAN_POINT('Ctrl Pts',(-26.7032662444742,22.8834215291061,-32.6508182123991));
#26302=CARTESIAN_POINT('Ctrl Pts',(-26.7045928509369,22.8897253096225,-32.6512209568453));
#26303=CARTESIAN_POINT('Ctrl Pts',(-26.7064442304517,22.8986554968719,-32.6517896146392));
#26304=CARTESIAN_POINT('Ctrl Pts',(-26.706984633214,22.9012785919598,-32.6519564183613));
#26305=CARTESIAN_POINT('Ctrl Pts',(-26.7079064211033,22.9057813100117,-32.6522423496674));
#26306=CARTESIAN_POINT('Ctrl Pts',(-26.7082893986772,22.9076606022992,-32.6523615693166));
#26307=CARTESIAN_POINT('Ctrl Pts',(-26.7090185778951,22.9112551219252,-32.6525893715429));
#26308=CARTESIAN_POINT('Ctrl Pts',(-26.7093650597716,22.9129702870776,-32.6526979703629));
#26309=CARTESIAN_POINT('Ctrl Pts',(-26.7101758934343,22.9170010114908,-32.6529529509841));
#26310=CARTESIAN_POINT('Ctrl Pts',(-26.7106390979575,22.9193168045582,-32.6530992664441));
#26311=CARTESIAN_POINT('Ctrl Pts',(-26.7119936293792,22.9261277091575,-32.6535290668989));
#26312=CARTESIAN_POINT('Ctrl Pts',(-26.712877919357,22.9306242392305,-32.6538121494546));
#26313=CARTESIAN_POINT('Ctrl Pts',(-26.7202770964689,22.9686768506077,-32.6562022343197));
#26314=CARTESIAN_POINT('Ctrl Pts',(-26.7262676317525,23.002334356276,-32.6582797953842));
#26315=CARTESIAN_POINT('Ctrl Pts',(-26.732688692665,23.0420651920247,-32.6606962001471));
#26316=CARTESIAN_POINT('Ctrl Pts',(-26.7336387208964,23.0480507172951,-32.6610592764642));
#26317=CARTESIAN_POINT('Ctrl Pts',(-26.736122052057,23.063986837241,-32.6620234787032));
#26318=CARTESIAN_POINT('Ctrl Pts',(-26.7376256315328,23.0739420723073,-32.6626232543491));
#26319=CARTESIAN_POINT('Ctrl Pts',(-26.7397098639901,23.0881937896272,-32.6634784331918));
#26320=CARTESIAN_POINT('Ctrl Pts',(-26.7403285234067,23.0924845521119,-32.6637354552184));
#26321=CARTESIAN_POINT('Ctrl Pts',(-26.7621486069362,23.2460120617907,-32.6729163913047));
#26322=CARTESIAN_POINT('Ctrl Pts',(-26.7728646033546,23.3965673596197,-32.6813997023904));
#26323=CARTESIAN_POINT('Ctrl Pts',(-26.7730983081691,23.6544965668712,-32.6958333340991));
#26324=CARTESIAN_POINT('Ctrl Pts',(-26.7678501364995,23.7615982352801,-32.7017964825508));
#26325=CARTESIAN_POINT('Ctrl Pts',(-26.7506351306255,23.9352193070715,-32.7116318662049));
#26326=CARTESIAN_POINT('Ctrl Pts',(-26.7418971322367,24.0019740988081,-32.7154538829357));
#26327=CARTESIAN_POINT('Ctrl Pts',(-26.7272066053712,24.0921561186822,-32.7207080397753));
#26328=CARTESIAN_POINT('Ctrl Pts',(-26.7230716017257,24.1158635265889,-32.7220978152095));
#26329=CARTESIAN_POINT('Ctrl Pts',(-26.6992670649057,24.2438571607339,-32.7296528838007));
#26330=CARTESIAN_POINT('Ctrl Pts',(-26.6747228249882,24.3471600573904,-32.7359402965192));
#26331=CARTESIAN_POINT('Ctrl Pts',(-26.6422408818053,24.4590060418438,-32.743028451979));
#26332=CARTESIAN_POINT('Ctrl Pts',(-26.6393035127819,24.4689412339944,-32.7436605290631));
#26333=CARTESIAN_POINT('Ctrl Pts',(-26.6350940429976,24.4829306462483,-32.7445540395965));
#26334=CARTESIAN_POINT('Ctrl Pts',(-26.6338617307538,24.4869968524253,-32.7448141686529));
#26335=CARTESIAN_POINT('Ctrl Pts',(-26.6317029885174,24.4940695382372,-32.7452673657088));
#26336=CARTESIAN_POINT('Ctrl Pts',(-26.6307801884695,24.4970771276101,-32.7454603143725));
#26337=CARTESIAN_POINT('Ctrl Pts',(-26.6288447772025,24.5033522381762,-32.7458633720861));
#26338=CARTESIAN_POINT('Ctrl Pts',(-26.6278313649448,24.5066195060229,-32.7460735072353));
#26339=CARTESIAN_POINT('Ctrl Pts',(-26.6254216518884,24.5143449910082,-32.7465710268662));
#26340=CARTESIAN_POINT('Ctrl Pts',(-26.6240208580881,24.5188017886722,-32.7468585589017));
#26341=CARTESIAN_POINT('Ctrl Pts',(-26.6193600234842,24.5335188575532,-32.7478097499679));
#26342=CARTESIAN_POINT('Ctrl Pts',(-26.6160582874658,24.5437657561116,-32.7484747818853));
#26343=CARTESIAN_POINT('Ctrl Pts',(-26.5624116192098,24.7074434511631,-32.7591423102099));
#26344=CARTESIAN_POINT('Ctrl Pts',(-26.5006647601484,24.8568688694441,-32.7695288225766));
#26345=CARTESIAN_POINT('Ctrl Pts',(-26.2897734951666,25.2751922328451,-32.8005351340332));
#26346=CARTESIAN_POINT('Ctrl Pts',(-26.1131001464262,25.5281771266788,-32.8219155330127));
#26347=CARTESIAN_POINT('Ctrl Pts',(-25.9002539487991,25.7556166851122,-32.8419988580087));
#26348=CARTESIAN_POINT('Ctrl Pts',(-25.8971800871024,25.758887576175,-32.8422878495362));
#26349=CARTESIAN_POINT('Ctrl Pts',(-25.8686389259693,25.7891313146573,-32.8449614133608));
#26350=CARTESIAN_POINT('Ctrl Pts',(-25.8427131489051,25.8156704383487,-32.8473182379716));
#26351=CARTESIAN_POINT('Ctrl Pts',(-25.8126738666521,25.845376440473,-32.8499625221209));
#26352=CARTESIAN_POINT('Ctrl Pts',(-25.809005488428,25.8489867779354,-32.8502840034902));
#26353=CARTESIAN_POINT('Ctrl Pts',(-25.8035757308584,25.8543050792307,-32.850757705815));
#26354=CARTESIAN_POINT('Ctrl Pts',(-25.8018210483055,25.8560198219475,-32.8509104592977));
#26355=CARTESIAN_POINT('Ctrl Pts',(-25.7987135074864,25.8590496996146,-32.8511804024676));
#26356=CARTESIAN_POINT('Ctrl Pts',(-25.7973614515446,25.8603656511454,-32.8512976569204));
#26357=CARTESIAN_POINT('Ctrl Pts',(-25.7945380250747,25.8631088585408,-32.8515421060299));
#26358=CARTESIAN_POINT('Ctrl Pts',(-25.7930664513423,25.8645358951399,-32.8516692833866));
#26359=CARTESIAN_POINT('Ctrl Pts',(-25.7892244627109,25.8682544999243,-32.8520007226058));
#26360=CARTESIAN_POINT('Ctrl Pts',(-25.7868518833875,25.8705438437574,-32.852204809072));
#26361=CARTESIAN_POINT('Ctrl Pts',(-25.7765702746411,25.8804343270815,-32.8530866926373));
#26362=CARTESIAN_POINT('Ctrl Pts',(-25.7686258563344,25.8879988166541,-32.8537616503768));
#26363=CARTESIAN_POINT('Ctrl Pts',(-25.7110509021562,25.9422625517316,-32.858608236146));
#26364=CARTESIAN_POINT('Ctrl Pts',(-25.6599846933156,25.9874216482024,-32.862667468548));
#26365=CARTESIAN_POINT('Ctrl Pts',(-25.5736481366165,26.0590219997102,-32.8692219328439));
#26366=CARTESIAN_POINT('Ctrl Pts',(-25.539202555839,26.0864173723997,-32.8717609163356));
#26367=CARTESIAN_POINT('Ctrl Pts',(-25.2722679819864,26.289932287134,-32.8909561791572));
#26368=CARTESIAN_POINT('Ctrl Pts',(-25.0174044632498,26.4344614285616,-32.9066944801757));
#26369=CARTESIAN_POINT('Ctrl Pts',(-24.6546546661541,26.5794786291965,-32.9294330246753));
#26370=CARTESIAN_POINT('Ctrl Pts',(-24.5611101796028,26.6119642424164,-32.9353093113016));
#26371=CARTESIAN_POINT('Ctrl Pts',(-24.4564622976942,26.6429867795241,-32.9419529435307));
#26372=CARTESIAN_POINT('Ctrl Pts',(-24.4466851313176,26.645834844973,-32.942574287992));
#26373=CARTESIAN_POINT('Ctrl Pts',(-24.4328399272386,26.649796827138,-32.9434551090364));
#26374=CARTESIAN_POINT('Ctrl Pts',(-24.4287828782563,26.6509491921378,-32.9437133304078));
#26375=CARTESIAN_POINT('Ctrl Pts',(-24.4217031938542,26.6529450968397,-32.9441641402112));
#26376=CARTESIAN_POINT('Ctrl Pts',(-24.4186815595877,26.6537921937244,-32.9443566124584));
#26377=CARTESIAN_POINT('Ctrl Pts',(-24.412462212064,26.6555259562327,-32.9447529086426));
#26378=CARTESIAN_POINT('Ctrl Pts',(-24.4092643583715,26.656412098678,-32.9449567493252));
#26379=CARTESIAN_POINT('Ctrl Pts',(-24.401684330326,26.6584999643181,-32.9454401002292));
#26380=CARTESIAN_POINT('Ctrl Pts',(-24.3973009802778,26.6596973592401,-32.9457197509294));
#26381=CARTESIAN_POINT('Ctrl Pts',(-24.3880341363292,26.6622077238328,-32.9463112630458));
#26382=CARTESIAN_POINT('Ctrl Pts',(-24.3831500594962,26.6635184764309,-32.9466231957879));
#26383=CARTESIAN_POINT('Ctrl Pts',(-24.3699818299296,26.6670192640124,-32.94746470178));
#26384=CARTESIAN_POINT('Ctrl Pts',(-24.3616920375857,26.6691877525778,-32.9479949734354));
#26385=CARTESIAN_POINT('Ctrl Pts',(-24.2135519161788,26.7073084662701,-32.9574805693437));
#26386=CARTESIAN_POINT('Ctrl Pts',(-24.0714703429511,26.7338495096319,-32.9667414510033));
#26387=CARTESIAN_POINT('Ctrl Pts',(-23.761737303224,26.7704164516937,-32.9872886600487));
#26388=CARTESIAN_POINT('Ctrl Pts',(-23.5941031360689,26.7770543971564,-32.998635131657));
#26389=CARTESIAN_POINT('Ctrl Pts',(-23.2402316804886,26.7634809317805,-33.0225962090429));
#26390=CARTESIAN_POINT('Ctrl Pts',(-23.0546837852011,26.7401395627148,-33.0351630026068));
#26391=CARTESIAN_POINT('Ctrl Pts',(-22.8610286743464,26.698461255551,-33.0476453019769));
#26392=CARTESIAN_POINT('Ctrl Pts',(-22.8498891122367,26.6960018517268,-33.0483609794725));
#26393=CARTESIAN_POINT('Ctrl Pts',(-22.8353607991941,26.6927132774818,-33.0492911047388));
#26394=CARTESIAN_POINT('Ctrl Pts',(-22.8319601846165,26.691937721591,-33.0495085831789));
#26395=CARTESIAN_POINT('Ctrl Pts',(-22.8267249640257,26.6907348146592,-33.0498430216029));
#26396=CARTESIAN_POINT('Ctrl Pts',(-22.8248894759949,26.6903113764076,-33.0499602072532));
#26397=CARTESIAN_POINT('Ctrl Pts',(-22.8212372389396,26.6894654496845,-33.0501932419281));
#26398=CARTESIAN_POINT('Ctrl Pts',(-22.8194204960659,26.6890429957548,-33.0503090917033));
#26399=CARTESIAN_POINT('Ctrl Pts',(-22.8153645231524,26.688096133036,-33.050567578188));
#26400=CARTESIAN_POINT('Ctrl Pts',(-22.8131254923378,26.6875709056418,-33.0507101665289));
#26401=CARTESIAN_POINT('Ctrl Pts',(-22.8065674786844,26.6860251317832,-33.0511274991716));
#26402=CARTESIAN_POINT('Ctrl Pts',(-22.80225001707,26.6849980550526,-33.0514018660614));
#26403=CARTESIAN_POINT('Ctrl Pts',(-22.77048408867,26.6773719252353,-33.0534178007276));
#26404=CARTESIAN_POINT('Ctrl Pts',(-22.7431201570533,26.6704211149257,-33.0551393464126));
#26405=CARTESIAN_POINT('Ctrl Pts',(-22.6534129253988,26.6463750698616,-33.060744148782));
#26406=CARTESIAN_POINT('Ctrl Pts',(-22.5914890045306,26.6277628467614,-33.0645508962943));
#26407=CARTESIAN_POINT('Ctrl Pts',(-22.3842433140677,26.5586081210394,-33.0772088376499));
#26408=CARTESIAN_POINT('Ctrl Pts',(-22.2419874796715,26.4995286688493,-33.0857651520371));
#26409=CARTESIAN_POINT('Ctrl Pts',(-22.0946437916706,26.4255685299444,-33.0949784066172));
#26410=CARTESIAN_POINT('Ctrl Pts',(-22.0848262603312,26.4205773674136,-33.0955939796048));
#26411=CARTESIAN_POINT('Ctrl Pts',(-22.0750360001986,26.4155367667575,-33.0962096862788));
#26412=CARTESIAN_POINT('',(-26.7730025278725,23.5500955840177,-32.9388531742191));
#26413=CARTESIAN_POINT('Ctrl Pts',(-22.0750360407425,26.4155367876319,-33.3457833635692));
#26414=CARTESIAN_POINT('Ctrl Pts',(-22.0934975599687,26.4250418611875,-33.3445398102641));
#26415=CARTESIAN_POINT('Ctrl Pts',(-22.112057404666,26.4343718359091,-33.3432898004641));
#26416=CARTESIAN_POINT('Ctrl Pts',(-22.1489865025916,26.4524905249892,-33.3408021499824));
#26417=CARTESIAN_POINT('Ctrl Pts',(-22.1673439408664,26.4612825304923,-33.3395653147227));
#26418=CARTESIAN_POINT('Ctrl Pts',(-22.1913318126899,26.4724930341881,-33.3379484153733));
#26419=CARTESIAN_POINT('Ctrl Pts',(-22.1968878667446,26.475070330772,-33.3375738612578));
#26420=CARTESIAN_POINT('Ctrl Pts',(-22.2058231341918,26.4791842375785,-33.3369714106402));
#26421=CARTESIAN_POINT('Ctrl Pts',(-22.2091977331234,26.4807308833716,-33.3367438611689));
#26422=CARTESIAN_POINT('Ctrl Pts',(-22.2155902487557,26.4836473461102,-33.3363127707687));
#26423=CARTESIAN_POINT('Ctrl Pts',(-22.2186076231808,26.4850183459017,-33.336109270969));
#26424=CARTESIAN_POINT('Ctrl Pts',(-22.2245590236632,26.4877114065796,-33.3357078550636));
#26425=CARTESIAN_POINT('Ctrl Pts',(-22.2274929262389,26.489033732283,-33.3355099483746));
#26426=CARTESIAN_POINT('Ctrl Pts',(-22.2365709503581,26.4931088981848,-33.33489753076));
#26427=CARTESIAN_POINT('Ctrl Pts',(-22.2427216921104,26.4958468678803,-33.3344825092304));
#26428=CARTESIAN_POINT('Ctrl Pts',(-22.2749532048219,26.5100737072113,-33.3323072071324));
#26429=CARTESIAN_POINT('Ctrl Pts',(-22.3011762800028,26.5212352306522,-33.3305357575639));
#26430=CARTESIAN_POINT('Ctrl Pts',(-22.609118704902,26.6475095361506,-33.309707762113));
#26431=CARTESIAN_POINT('Ctrl Pts',(-22.9055735821883,26.7224815967412,-33.2891878761496));
#26432=CARTESIAN_POINT('Ctrl Pts',(-23.3588341836674,26.7708850918646,-33.2583693139221));
#26433=CARTESIAN_POINT('Ctrl Pts',(-23.5105910648775,26.7763262353634,-33.2481853320502));
#26434=CARTESIAN_POINT('Ctrl Pts',(-23.6694572013835,26.7708054078662,-33.2379986315153));
#26435=CARTESIAN_POINT('Ctrl Pts',(-23.6767334181999,26.7705278567195,-33.2375331354797));
#26436=CARTESIAN_POINT('Ctrl Pts',(-23.686994732268,26.7701016065472,-33.2368782269043));
#26437=CARTESIAN_POINT('Ctrl Pts',(-23.6899805990014,26.7699734142563,-33.2366878459587));
#26438=CARTESIAN_POINT('Ctrl Pts',(-23.7051621395935,26.7693004665252,-33.2357208218588));
#26439=CARTESIAN_POINT('Ctrl Pts',(-23.7173550338048,26.7686905624561,-33.2349473217719));
#26440=CARTESIAN_POINT('Ctrl Pts',(-23.7418179867142,26.7673274994166,-33.2334021530993));
#26441=CARTESIAN_POINT('Ctrl Pts',(-23.754087812286,26.7665733896745,-33.2326305457675));
#26442=CARTESIAN_POINT('Ctrl Pts',(-23.7699363465307,26.7655082727707,-33.2316385410066));
#26443=CARTESIAN_POINT('Ctrl Pts',(-23.7735190531659,26.7652614772053,-33.2314145968123));
#26444=CARTESIAN_POINT('Ctrl Pts',(-23.7790011998562,26.7648746302738,-33.2310724028891));
#26445=CARTESIAN_POINT('Ctrl Pts',(-23.7809009256648,26.7647388838606,-33.2309539105454));
#26446=CARTESIAN_POINT('Ctrl Pts',(-23.7844735270852,26.7644804174183,-33.2307312421432));
#26447=CARTESIAN_POINT('Ctrl Pts',(-23.7861464203984,26.7643580759092,-33.2306270452211));
#26448=CARTESIAN_POINT('Ctrl Pts',(-23.790000794754,26.7640731735606,-33.2303871325266));
#26449=CARTESIAN_POINT('Ctrl Pts',(-23.7921822023698,26.7639096979523,-33.2302514693569));
#26450=CARTESIAN_POINT('Ctrl Pts',(-23.7982668146116,26.7634474840974,-33.229873385367));
#26451=CARTESIAN_POINT('Ctrl Pts',(-23.802169660645,26.7631438537291,-33.2296312410973));
#26452=CARTESIAN_POINT('Ctrl Pts',(-23.8241538716531,26.7613932397491,-33.2282693092708));
#26453=CARTESIAN_POINT('Ctrl Pts',(-23.8422237931861,26.7598006945302,-33.2271576244526));
#26454=CARTESIAN_POINT('Ctrl Pts',(-23.8946149664489,26.7547372003608,-33.2239544766026));
#26455=CARTESIAN_POINT('Ctrl Pts',(-23.9288961922194,26.7508675772511,-33.2218835248355));
#26456=CARTESIAN_POINT('Ctrl Pts',(-24.0637070796941,26.7334538410463,-33.213814867673));
#26457=CARTESIAN_POINT('Ctrl Pts',(-24.1636431018701,26.7157164090414,-33.207998293565));
#26458=CARTESIAN_POINT('Ctrl Pts',(-24.3350497976686,26.6768692232602,-33.1980603507916));
#26459=CARTESIAN_POINT('Ctrl Pts',(-24.406928029046,26.6579439916959,-33.1939050691083));
#26460=CARTESIAN_POINT('Ctrl Pts',(-24.5557749688265,26.6131960086862,-33.1852193643978));
#26461=CARTESIAN_POINT('Ctrl Pts',(-24.6325506385452,26.5869165973926,-33.1806924514923));
#26462=CARTESIAN_POINT('Ctrl Pts',(-24.8947824507328,26.4859481403797,-33.1648687780428));
#26463=CARTESIAN_POINT('Ctrl Pts',(-25.0741970084934,26.3969426085533,-33.1533661924852));
#26464=CARTESIAN_POINT('Ctrl Pts',(-25.2546006401569,26.2854791351249,-33.1404768623262));
#26465=CARTESIAN_POINT('Ctrl Pts',(-25.2649650808094,26.2789936176864,-33.1397315731207));
#26466=CARTESIAN_POINT('Ctrl Pts',(-25.2794874153284,26.2697909017924,-33.138680459494));
#26467=CARTESIAN_POINT('Ctrl Pts',(-25.2836764058192,26.2671227717664,-33.1383764589223));
#26468=CARTESIAN_POINT('Ctrl Pts',(-25.2907595637828,26.2625881845202,-33.1378610523619));
#26469=CARTESIAN_POINT('Ctrl Pts',(-25.2936569469994,26.2607267460871,-33.1376498337871));
#26470=CARTESIAN_POINT('Ctrl Pts',(-25.2992164416482,26.2571424185173,-33.1372437950153));
#26471=CARTESIAN_POINT('Ctrl Pts',(-25.3018790061255,26.2554202365997,-33.137049001431));
#26472=CARTESIAN_POINT('Ctrl Pts',(-25.3073590406735,26.2518641950922,-33.1366473932997));
#26473=CARTESIAN_POINT('Ctrl Pts',(-25.3101761908232,26.250029851698,-33.1364405607687));
#26474=CARTESIAN_POINT('Ctrl Pts',(-25.3198341616743,26.2437196741262,-33.135730186922));
#26475=CARTESIAN_POINT('Ctrl Pts',(-25.3266607765907,26.2392222485213,-33.1352258348168));
#26476=CARTESIAN_POINT('Ctrl Pts',(-25.3805809713667,26.2034042706858,-33.131224345914));
#26477=CARTESIAN_POINT('Ctrl Pts',(-25.4268572011357,26.1708766186661,-33.1276816819474));
#26478=CARTESIAN_POINT('Ctrl Pts',(-25.5830425041545,26.0548349136855,-33.115334003637));
#26479=CARTESIAN_POINT('Ctrl Pts',(-25.6884173178196,25.965498047776,-33.1063052792513));
#26480=CARTESIAN_POINT('Ctrl Pts',(-25.9920850967049,25.6725608507018,-33.078148817936));
#26481=CARTESIAN_POINT('Ctrl Pts',(-26.1694835395828,25.4492962584218,-33.0584568692416));
#26482=CARTESIAN_POINT('Ctrl Pts',(-26.3335683822166,25.1752234889727,-33.0379419277616));
#26483=CARTESIAN_POINT('Ctrl Pts',(-26.3512995679964,25.1444650320273,-33.0356881699773));
#26484=CARTESIAN_POINT('Ctrl Pts',(-26.3707675269096,25.1093658051939,-33.0331761749419));
#26485=CARTESIAN_POINT('Ctrl Pts',(-26.3730065522511,25.1053084078306,-33.0328866870299));
#26486=CARTESIAN_POINT('Ctrl Pts',(-26.3763798428218,25.0991642865995,-33.0324496814402));
#26487=CARTESIAN_POINT('Ctrl Pts',(-26.3775205538046,25.0970811370757,-33.0323017527223));
#26488=CARTESIAN_POINT('Ctrl Pts',(-26.3794993398527,25.0934580056666,-33.032044880958));
#26489=CARTESIAN_POINT('Ctrl Pts',(-26.3803384609108,25.0919186011326,-33.0319358704661));
#26490=CARTESIAN_POINT('Ctrl Pts',(-26.3820915109339,25.0886962991249,-33.0317079609219));
#26491=CARTESIAN_POINT('Ctrl Pts',(-26.38300519554,25.0870132727936,-33.0315890780516));
#26492=CARTESIAN_POINT('Ctrl Pts',(-26.3851855519611,25.0829884585597,-33.0313051491347));
#26493=CARTESIAN_POINT('Ctrl Pts',(-26.3864508268256,25.0806459065231,-33.0311401932215));
#26494=CARTESIAN_POINT('Ctrl Pts',(-26.3907233234603,25.0727122347591,-33.0305825267814));
#26495=CARTESIAN_POINT('Ctrl Pts',(-26.3937169515039,25.0671137518563,-33.0301906827581));
#26496=CARTESIAN_POINT('Ctrl Pts',(-26.4007886855405,25.053794164906,-33.0292623257062));
#26497=CARTESIAN_POINT('Ctrl Pts',(-26.4048520181897,25.0460652147992,-33.0287267258366));
#26498=CARTESIAN_POINT('Ctrl Pts',(-26.4521185598003,24.9552644636975,-33.0224695368331));
#26499=CARTESIAN_POINT('Ctrl Pts',(-26.4917176430043,24.8703554270289,-33.0169616360652));
#26500=CARTESIAN_POINT('Ctrl Pts',(-26.6501299219583,24.4880190416136,-32.9931300871853));
#26501=CARTESIAN_POINT('Ctrl Pts',(-26.7279281297272,24.1755919286179,-32.9759853056577));
#26502=CARTESIAN_POINT('Ctrl Pts',(-26.7613682438287,23.8256322036592,-32.9554157090191));
#26503=CARTESIAN_POINT('Ctrl Pts',(-26.7638922506264,23.7944199831725,-32.9535715425229));
#26504=CARTESIAN_POINT('Ctrl Pts',(-26.7697429750524,23.7060588179885,-32.9483184815699));
#26505=CARTESIAN_POINT('Ctrl Pts',(-26.7720022991397,23.648853342671,-32.9448793374993));
#26506=CARTESIAN_POINT('Ctrl Pts',(-26.7728495196694,23.5828567386286,-32.9408577584136));
#26507=CARTESIAN_POINT('Ctrl Pts',(-26.7729262718921,23.5740924785577,-32.9403226086109));
#26508=CARTESIAN_POINT('Ctrl Pts',(-26.7729869265949,23.5611262650312,-32.9395292387437));
#26509=CARTESIAN_POINT('Ctrl Pts',(-26.7729983646242,23.5569244294693,-32.9392718832151));
#26510=CARTESIAN_POINT('Ctrl Pts',(-26.7730022562627,23.5518469269387,-32.9389605824208));
#26511=CARTESIAN_POINT('Ctrl Pts',(-26.7730025705176,23.5509712551186,-32.9389068839172));
#26512=CARTESIAN_POINT('Ctrl Pts',(-26.7730025278725,23.5500955840177,-32.9388531742191));
#26513=CARTESIAN_POINT('Ctrl Pts',(-26.7730025278685,23.5500955013274,-32.9388531691472));
#26514=CARTESIAN_POINT('Ctrl Pts',(-26.7730024448801,23.5483923217316,-32.9387487038255));
#26515=CARTESIAN_POINT('Ctrl Pts',(-26.7730010117309,23.5466891448804,-32.9386441961556));
#26516=CARTESIAN_POINT('Ctrl Pts',(-26.772992709127,23.5416085639561,-32.9383323222094));
#26517=CARTESIAN_POINT('Ctrl Pts',(-26.7729818806004,23.5382311766048,-32.9381248318214));
#26518=CARTESIAN_POINT('Ctrl Pts',(-26.7729435256734,23.53020407965,-32.9376312840049));
#26519=CARTESIAN_POINT('Ctrl Pts',(-26.7729112454758,23.5255544097048,-32.937345077671));
#26520=CARTESIAN_POINT('Ctrl Pts',(-26.7727734305524,23.5104212021922,-32.9364125139594));
#26521=CARTESIAN_POINT('Ctrl Pts',(-26.7726268024879,23.4999381883714,-32.9357648679799));
#26522=CARTESIAN_POINT('Ctrl Pts',(-26.7722380264066,23.4793332504897,-32.9344885898365));
#26523=CARTESIAN_POINT('Ctrl Pts',(-26.7719993249735,23.4692113766779,-32.9338600736771));
#26524=CARTESIAN_POINT('Ctrl Pts',(-26.7612907049837,23.0907913105067,-32.9103027448846));
#26525=CARTESIAN_POINT('Ctrl Pts',(-26.6877808583376,22.7270685989479,-32.885084236381));
#26526=CARTESIAN_POINT('Ctrl Pts',(-26.5081357901743,22.264385823112,-32.8518196064956));
#26527=CARTESIAN_POINT('Ctrl Pts',(-26.4546867999505,22.1478272357721,-32.8433775225756));
#26528=CARTESIAN_POINT('Ctrl Pts',(-26.3906799218286,22.0277041755948,-32.8348313886617));
#26529=CARTESIAN_POINT('Ctrl Pts',(-26.3869007472472,22.0206747599834,-32.8343318763894));
#26530=CARTESIAN_POINT('Ctrl Pts',(-26.3817036798259,22.0110935149354,-32.8336519194398));
#26531=CARTESIAN_POINT('Ctrl Pts',(-26.3803084160115,22.008529542656,-32.8334700480098));
#26532=CARTESIAN_POINT('Ctrl Pts',(-26.377967191008,22.0042411357324,-32.8331660071871));
#26533=CARTESIAN_POINT('Ctrl Pts',(-26.3770231348408,22.0025156715728,-32.8330437155999));
#26534=CARTESIAN_POINT('Ctrl Pts',(-26.375160036499,21.9991178524422,-32.832802978814));
#26535=CARTESIAN_POINT('Ctrl Pts',(-26.374241088537,21.9974454494284,-32.832684527838));
#26536=CARTESIAN_POINT('Ctrl Pts',(-26.3722108462576,21.9937583533224,-32.8324234673793));
#26537=CARTESIAN_POINT('Ctrl Pts',(-26.3710988767487,21.9917440286347,-32.8322809014323));
#26538=CARTESIAN_POINT('Ctrl Pts',(-26.3672025955125,21.9847037740034,-32.831782809551));
#26539=CARTESIAN_POINT('Ctrl Pts',(-26.3644069798813,21.979684062092,-32.831428007475));
#26540=CARTESIAN_POINT('Ctrl Pts',(-26.3358112527086,21.9286600398056,-32.8278247092542));
#26541=CARTESIAN_POINT('Ctrl Pts',(-26.308897036284,21.8832849595732,-32.8246465990569));
#26542=CARTESIAN_POINT('Ctrl Pts',(-26.2014680084607,21.7119029247497,-32.8126641634843));
#26543=CARTESIAN_POINT('Ctrl Pts',(-26.1133285652527,21.5908845319508,-32.8042430819917));
#26544=CARTESIAN_POINT('Ctrl Pts',(-25.9110167258903,21.3502333460017,-32.7866458254143));
#26545=CARTESIAN_POINT('Ctrl Pts',(-25.7954145153002,21.2323791317175,-32.7775002353527));
#26546=CARTESIAN_POINT('Ctrl Pts',(-25.606450882027,21.0671924849104,-32.7631272586304));
#26547=CARTESIAN_POINT('Ctrl Pts',(-25.5393491364183,21.0131219001765,-32.7581226245599));
#26548=CARTESIAN_POINT('Ctrl Pts',(-25.4224763846164,20.9264345351844,-32.7494949431218));
#26549=CARTESIAN_POINT('Ctrl Pts',(-25.3738212384152,20.8923888211743,-32.7459277758914));
#26550=CARTESIAN_POINT('Ctrl Pts',(-25.3173524649615,20.8551562880726,-32.7418043631227));
#26551=CARTESIAN_POINT('Ctrl Pts',(-25.3104316852225,20.8506312097284,-32.741299283889));
#26552=CARTESIAN_POINT('Ctrl Pts',(-25.3006646363791,20.8442986529883,-32.7405868543038));
#26553=CARTESIAN_POINT('Ctrl Pts',(-25.2978327870509,20.8424689028085,-32.7403803367974));
#26554=CARTESIAN_POINT('Ctrl Pts',(-25.2921745512692,20.8388255055654,-32.7399677847452));
#26555=CARTESIAN_POINT('Ctrl Pts',(-25.2893481908711,20.8370118257493,-32.7397617517658));
#26556=CARTESIAN_POINT('Ctrl Pts',(-25.2838747350031,20.8335115667915,-32.7393628324769));
#26557=CARTESIAN_POINT('Ctrl Pts',(-25.2812279991285,20.8318244297908,-32.7391699672304));
#26558=CARTESIAN_POINT('Ctrl Pts',(-25.2744888667233,20.8275424655377,-32.7386789806575));
#26559=CARTESIAN_POINT('Ctrl Pts',(-25.2703930854803,20.8249530035332,-32.7383806604875));
#26560=CARTESIAN_POINT('Ctrl Pts',(-25.2565231158068,20.8162277624099,-32.7373706942528));
#26561=CARTESIAN_POINT('Ctrl Pts',(-25.2467219008516,20.8101353044184,-32.7366574473003));
#26562=CARTESIAN_POINT('Ctrl Pts',(-25.0840016412879,20.7101957083805,-32.7248227451569));
#26563=CARTESIAN_POINT('Ctrl Pts',(-24.9235684379159,20.6292436815508,-32.7132238326056));
#26564=CARTESIAN_POINT('Ctrl Pts',(-24.6404389462193,20.5148803099678,-32.6928995698178));
#26565=CARTESIAN_POINT('Ctrl Pts',(-24.5209578058768,20.4745868465639,-32.6843706171678));
#26566=CARTESIAN_POINT('Ctrl Pts',(-24.3692103295671,20.4331373367921,-32.6737237044016));
#26567=CARTESIAN_POINT('Ctrl Pts',(-24.3388704104149,20.4253235925019,-32.6716043753079));
#26568=CARTESIAN_POINT('Ctrl Pts',(-24.2080795937979,20.3936658543684,-32.6625180722159));
#26569=CARTESIAN_POINT('Ctrl Pts',(-24.1066219995136,20.3742122802831,-32.6555931572272));
#26570=CARTESIAN_POINT('Ctrl Pts',(-23.962112668255,20.3536428876116,-32.6460414567569));
#26571=CARTESIAN_POINT('Ctrl Pts',(-23.9197078361218,20.3484647264754,-32.6432763534145));
#26572=CARTESIAN_POINT('Ctrl Pts',(-23.8505028150485,20.3414072492971,-32.6388381056639));
#26573=CARTESIAN_POINT('Ctrl Pts',(-23.8237610920042,20.3390173390903,-32.6371411308387));
#26574=CARTESIAN_POINT('Ctrl Pts',(-23.7926236343889,20.3366263862805,-32.6351885805348));
#26575=CARTESIAN_POINT('Ctrl Pts',(-23.788254982577,20.3362998892579,-32.6349151680174));
#26576=CARTESIAN_POINT('Ctrl Pts',(-23.7816037929846,20.3358164395047,-32.6344997301326));
#26577=CARTESIAN_POINT('Ctrl Pts',(-23.7793217535862,20.3356530094316,-32.634357340617));
#26578=CARTESIAN_POINT('Ctrl Pts',(-23.7751794865671,20.3353607909874,-32.634099152264));
#26579=CARTESIAN_POINT('Ctrl Pts',(-23.7733193275193,20.3352311874189,-32.6339833076684));
#26580=CARTESIAN_POINT('Ctrl Pts',(-23.7695725095829,20.3349734014089,-32.6337501686745));
#26581=CARTESIAN_POINT('Ctrl Pts',(-23.767685857983,20.3348452655748,-32.6336328773225));
#26582=CARTESIAN_POINT('Ctrl Pts',(-23.7622831977847,20.3344831095852,-32.6332972887105));
#26583=CARTESIAN_POINT('Ctrl Pts',(-23.7587669026956,20.3342531944893,-32.6330792237633));
#26584=CARTESIAN_POINT('Ctrl Pts',(-23.7435657184972,20.3332842918002,-32.6321380050906));
#26585=CARTESIAN_POINT('Ctrl Pts',(-23.7318770359504,20.3326032043024,-32.6314180791118));
#26586=CARTESIAN_POINT('Ctrl Pts',(-23.5315262038528,20.3220242024919,-32.6191393906247));
#26587=CARTESIAN_POINT('Ctrl Pts',(-23.3423248994838,20.3286694074378,-32.6084640003419));
#26588=CARTESIAN_POINT('Ctrl Pts',(-22.9894404253086,20.3723035744781,-32.588549400399));
#26589=CARTESIAN_POINT('Ctrl Pts',(-22.8259454551091,20.4055352459347,-32.579316486071));
#26590=CARTESIAN_POINT('Ctrl Pts',(-22.5244372085474,20.4915895526733,-32.5613824465345));
#26591=CARTESIAN_POINT('Ctrl Pts',(-22.3860584891629,20.5415385895365,-32.5527696868908));
#26592=CARTESIAN_POINT('Ctrl Pts',(-22.2427341036593,20.6046445157459,-32.5432328128197));
#26593=CARTESIAN_POINT('Ctrl Pts',(-22.2339039198737,20.6085799883571,-32.5426427231619));
#26594=CARTESIAN_POINT('Ctrl Pts',(-22.2218846027218,20.6140017614471,-32.541836020847));
#26595=CARTESIAN_POINT('Ctrl Pts',(-22.2186799344322,20.6154536700064,-32.5416205926686));
#26596=CARTESIAN_POINT('Ctrl Pts',(-22.2123383413912,20.6183393205256,-32.5411936136187));
#26597=CARTESIAN_POINT('Ctrl Pts',(-22.2092013276468,20.619772856553,-32.5409820700677));
#26598=CARTESIAN_POINT('Ctrl Pts',(-22.2030012036241,20.622618197052,-32.5405633135635));
#26599=CARTESIAN_POINT('Ctrl Pts',(-22.19993799602,20.624029779925,-32.5403561084788));
#26600=CARTESIAN_POINT('Ctrl Pts',(-22.1926742368548,20.6273908891914,-32.5398640115575));
#26601=CARTESIAN_POINT('Ctrl Pts',(-22.1884756686862,20.6293446620667,-32.5395789729213));
#26602=CARTESIAN_POINT('Ctrl Pts',(-22.174877681297,20.635708077134,-32.5386538597012));
#26603=CARTESIAN_POINT('Ctrl Pts',(-22.1654954290017,20.6401540592701,-32.5380125249133));
#26604=CARTESIAN_POINT('Ctrl Pts',(-22.0596522341203,20.6909378882987,-32.530742791405));
#26605=CARTESIAN_POINT('Ctrl Pts',(-21.9655456909224,20.7420023059026,-32.5239489342222));
#26606=CARTESIAN_POINT('Ctrl Pts',(-21.7250115949532,20.8884661623284,-32.5056650793883));
#26607=CARTESIAN_POINT('Ctrl Pts',(-21.583506544014,20.9912471509419,-32.493936398287));
#26608=CARTESIAN_POINT('Ctrl Pts',(-21.4269881206853,21.1256143325353,-32.4799772255557));
#26609=CARTESIAN_POINT('Ctrl Pts',(-21.4032449580152,21.1466134917307,-32.4778310510643));
#26610=CARTESIAN_POINT('Ctrl Pts',(-21.354467102715,21.1910535601611,-32.4733659870379));
#26611=CARTESIAN_POINT('Ctrl Pts',(-21.3294887965583,21.2145509442134,-32.4710476107752));
#26612=CARTESIAN_POINT('Ctrl Pts',(-21.274714305742,21.2677510737375,-32.4658983630617));
#26613=CARTESIAN_POINT('Ctrl Pts',(-21.2451146244644,21.297648150091,-32.4630709088906));
#26614=CARTESIAN_POINT('Ctrl Pts',(-21.1706952015629,21.3758187445105,-32.4558609967869));
#26615=CARTESIAN_POINT('Ctrl Pts',(-21.1267524101377,21.4249046598426,-32.4515049641448));
#26616=CARTESIAN_POINT('Ctrl Pts',(-21.0657346745248,21.4974194034751,-32.4453489385222));
#26617=CARTESIAN_POINT('Ctrl Pts',(-21.0474245075924,21.5197834132823,-32.443486805763));
#26618=CARTESIAN_POINT('Ctrl Pts',(-21.0127552722545,21.5633100515964,-32.4399367798627));
#26619=CARTESIAN_POINT('Ctrl Pts',(-20.9963538856645,21.5844360140202,-32.4382463935143));
#26620=CARTESIAN_POINT('Ctrl Pts',(-20.977576189165,21.6092545533601,-32.4363005695847));
#26621=CARTESIAN_POINT('Ctrl Pts',(-20.9749427294391,21.612749979888,-32.4360274333464));
#26622=CARTESIAN_POINT('Ctrl Pts',(-20.9709439626368,21.6180801537199,-32.4356123289803));
#26623=CARTESIAN_POINT('Ctrl Pts',(-20.9695734882036,21.6199109901045,-32.4354699975957));
#26624=CARTESIAN_POINT('Ctrl Pts',(-20.9670891588567,21.6232372155766,-32.4352118703271));
#26625=CARTESIAN_POINT('Ctrl Pts',(-20.9659746566322,21.6247321075389,-32.4350960287873));
#26626=CARTESIAN_POINT('Ctrl Pts',(-20.9635617626,21.6279744126945,-32.434845140499));
#26627=CARTESIAN_POINT('Ctrl Pts',(-20.9622638473796,21.6297221696251,-32.4347101276146));
#26628=CARTESIAN_POINT('Ctrl Pts',(-20.9587261818786,21.6344960454671,-32.4343419667466));
#26629=CARTESIAN_POINT('Ctrl Pts',(-20.9564899527783,21.6375247881644,-32.4341090663784));
#26630=CARTESIAN_POINT('Ctrl Pts',(-20.9457494194838,21.6521252105784,-32.4329895551772));
#26631=CARTESIAN_POINT('Ctrl Pts',(-20.9373170430352,21.6637499637321,-32.4321079066826));
#26632=CARTESIAN_POINT('Ctrl Pts',(-20.7854078230201,21.8761425095127,-32.4161672995348));
#26633=CARTESIAN_POINT('Ctrl Pts',(-20.6653543271839,22.0927148868873,-32.402584711569));
#26634=CARTESIAN_POINT('Ctrl Pts',(-20.5157421235767,22.4552672554377,-32.3806514408196));
#26635=CARTESIAN_POINT('Ctrl Pts',(-20.4694512672832,22.593223081863,-32.3724796837955));
#26636=CARTESIAN_POINT('Ctrl Pts',(-20.4081303995654,22.8273833972928,-32.3584314549032));
#26637=CARTESIAN_POINT('Ctrl Pts',(-20.387855446206,22.9219905029053,-32.3527115057707));
#26638=CARTESIAN_POINT('Ctrl Pts',(-20.368984280358,23.0345456970131,-32.3457961172374));
#26639=CARTESIAN_POINT('Ctrl Pts',(-20.3662423233057,23.0517545873036,-32.3447358629701));
#26640=CARTESIAN_POINT('Ctrl Pts',(-20.363011548495,23.0731464704354,-32.3434139987673));
#26641=CARTESIAN_POINT('Ctrl Pts',(-20.3623911469561,23.0773095434755,-32.3431565683048));
#26642=CARTESIAN_POINT('Ctrl Pts',(-20.36120745584,23.0853606082667,-32.3426583597296));
#26643=CARTESIAN_POINT('Ctrl Pts',(-20.3606431161796,23.0892484400211,-32.3424176153482));
#26644=CARTESIAN_POINT('Ctrl Pts',(-20.3596368733398,23.0962709192129,-32.3419824711307));
#26645=CARTESIAN_POINT('Ctrl Pts',(-20.3591924765587,23.0994052091849,-32.3417881506289));
#26646=CARTESIAN_POINT('Ctrl Pts',(-20.3582861849751,23.1058656724,-32.3413873929794));
#26647=CARTESIAN_POINT('Ctrl Pts',(-20.3578248696292,23.1091919217463,-32.3411809377242));
#26648=CARTESIAN_POINT('Ctrl Pts',(-20.3565688157848,23.1183537348506,-32.3406119436688));
#26649=CARTESIAN_POINT('Ctrl Pts',(-20.3557848764421,23.1241907441664,-32.3402490631975));
#26650=CARTESIAN_POINT('Ctrl Pts',(-20.3526121809303,23.1483148806608,-32.3387477260275));
#26651=CARTESIAN_POINT('Ctrl Pts',(-20.3503644586864,23.1666199136702,-32.3376048154102));
#26652=CARTESIAN_POINT('Ctrl Pts',(-20.3032741230911,23.5793718432674,-32.3117465916405));
#26653=CARTESIAN_POINT('Ctrl Pts',(-20.3315604187292,23.9786734206678,-32.2843093577868));
#26654=CARTESIAN_POINT('Ctrl Pts',(-20.4392175007159,24.3919768048705,-32.2559392313534));
#26655=CARTESIAN_POINT('Ctrl Pts',(-20.4472826421083,24.4212385718692,-32.253934274045));
#26656=CARTESIAN_POINT('Ctrl Pts',(-20.4697908015396,24.4986177343839,-32.2486492499378));
#26657=CARTESIAN_POINT('Ctrl Pts',(-20.4849481944475,24.5465210535561,-32.2453948329886));
#26658=CARTESIAN_POINT('Ctrl Pts',(-20.5090014674843,24.6167827500001,-32.2406666758664));
#26659=CARTESIAN_POINT('Ctrl Pts',(-20.5170368694584,24.6394254161046,-32.2391500367616));
#26660=CARTESIAN_POINT('Ctrl Pts',(-20.5267917606022,24.665967821038,-32.2373823008174));
#26661=CARTESIAN_POINT('Ctrl Pts',(-20.5282664109006,24.6699558528619,-32.2371169664158));
#26662=CARTESIAN_POINT('Ctrl Pts',(-20.5305371508951,24.6760596606071,-32.236711290985));
#26663=CARTESIAN_POINT('Ctrl Pts',(-20.5313275741362,24.6781775173447,-32.236570611438));
#26664=CARTESIAN_POINT('Ctrl Pts',(-20.5327675149939,24.6820233318838,-32.236315297225));
#26665=CARTESIAN_POINT('Ctrl Pts',(-20.5334162863201,24.6837515563149,-32.2362006183124));
#26666=CARTESIAN_POINT('Ctrl Pts',(-20.534736934515,24.6872603890066,-32.2359678935264));
#26667=CARTESIAN_POINT('Ctrl Pts',(-20.5354089011075,24.6890409525952,-32.2358498537634));
#26668=CARTESIAN_POINT('Ctrl Pts',(-20.5373508916225,24.6941730338864,-32.2355097913419));
#26669=CARTESIAN_POINT('Ctrl Pts',(-20.5386249348863,24.6975230431797,-32.235288010993));
#26670=CARTESIAN_POINT('Ctrl Pts',(-20.5442710332671,24.7122948568668,-32.2343109200981));
#26671=CARTESIAN_POINT('Ctrl Pts',(-20.5487025708757,24.7236940421205,-32.2335591480033));
#26672=CARTESIAN_POINT('Ctrl Pts',(-20.5547533042494,24.738999693843,-32.2325524044189));
#26673=CARTESIAN_POINT('Ctrl Pts',(-20.5563153774292,24.7429284113427,-32.2322942259462));
#26674=CARTESIAN_POINT('Ctrl Pts',(-20.678673881811,25.0489129699255,-32.2122038405596));
#26675=CARTESIAN_POINT('Ctrl Pts',(-20.8445229843576,25.3309994501408,-32.1948762701202));
#26676=CARTESIAN_POINT('Ctrl Pts',(-21.0997007465806,25.6448067668107,-32.1719248236123));
#26677=CARTESIAN_POINT('Ctrl Pts',(-21.1517893618659,25.7042568936529,-32.1673917865189));
#26678=CARTESIAN_POINT('Ctrl Pts',(-21.264216841234,25.8234340142811,-32.1578302418444));
#26679=CARTESIAN_POINT('Ctrl Pts',(-21.3248350630511,25.8828108690017,-32.1527934724041));
#26680=CARTESIAN_POINT('Ctrl Pts',(-21.3996273160094,25.9504997317078,-32.1466760200205));
#26681=CARTESIAN_POINT('Ctrl Pts',(-21.4116139476544,25.9611860504339,-32.1456984676126));
#26682=CARTESIAN_POINT('Ctrl Pts',(-21.4267636816768,25.9744904555619,-32.1444663326936));
#26683=CARTESIAN_POINT('Ctrl Pts',(-21.4298527449872,25.9771928177238,-32.1442152725309));
#26684=CARTESIAN_POINT('Ctrl Pts',(-21.435388514586,25.9820169610702,-32.1437656670329));
#26685=CARTESIAN_POINT('Ctrl Pts',(-21.4378332770202,25.9841409726871,-32.1435672147236));
#26686=CARTESIAN_POINT('Ctrl Pts',(-21.442768759651,25.9884158861818,-32.1431667927152));
#26687=CARTESIAN_POINT('Ctrl Pts',(-21.4452595808544,25.9905666650337,-32.1429648182638));
#26688=CARTESIAN_POINT('Ctrl Pts',(-21.4502401611088,25.9948540063139,-32.1425611707035));
#26689=CARTESIAN_POINT('Ctrl Pts',(-21.45272989724,25.9969905896301,-32.1423594987949));
#26690=CARTESIAN_POINT('Ctrl Pts',(-21.4594261472661,26.0027192880005,-32.1418173777458));
#26691=CARTESIAN_POINT('Ctrl Pts',(-21.4636386401292,26.0063043689985,-32.141476639139));
#26692=CARTESIAN_POINT('Ctrl Pts',(-21.4799286346328,26.020095960544,-32.1401601164727));
#26693=CARTESIAN_POINT('Ctrl Pts',(-21.492071805969,26.0302242427611,-32.1391811315167));
#26694=CARTESIAN_POINT('Ctrl Pts',(-21.6808000738247,26.1852963789888,-32.1240010788068));
#26695=CARTESIAN_POINT('Ctrl Pts',(-21.8721373965565,26.3110726560551,-32.1090129910853));
#26696=CARTESIAN_POINT('Ctrl Pts',(-22.0750360188393,26.4155367763548,-32.0936416103654));
#26697=CARTESIAN_POINT('Origin',(-23.5502525316942,23.5502525316942,-77.3107734492734));
#26698=CARTESIAN_POINT('',(-22.0750360141079,26.4155367739188,-30.5945512678406));
#26699=CARTESIAN_POINT('',(-22.0750360153473,26.4155367745569,-30.8398067994259));
#26700=CARTESIAN_POINT('',(-22.0750360153461,26.4155367745563,-77.3107734492734));
#26701=CARTESIAN_POINT('',(-26.7730022123545,23.5516872106683,-31.4417267961338));
#26702=CARTESIAN_POINT('Ctrl Pts',(-22.0750360141079,26.4155367739188,-30.5945512678406));
#26703=CARTESIAN_POINT('Ctrl Pts',(-22.0688193424089,26.4123360664149,-30.5950155140757));
#26704=CARTESIAN_POINT('Ctrl Pts',(-22.062612960042,26.4091150613421,-30.5954802403181));
#26705=CARTESIAN_POINT('Ctrl Pts',(-21.899720217809,26.3239024409474,-30.6077100556798));
#26706=CARTESIAN_POINT('Ctrl Pts',(-21.7500411724996,26.2291746960651,-30.6197661635553));
#26707=CARTESIAN_POINT('Ctrl Pts',(-21.5169744860561,26.0532828368445,-30.6394290545501));
#26708=CARTESIAN_POINT('Ctrl Pts',(-21.4288260479307,25.9790248359596,-30.6471016274814));
#26709=CARTESIAN_POINT('Ctrl Pts',(-21.3166967554925,25.873791936247,-30.6569980997168));
#26710=CARTESIAN_POINT('Ctrl Pts',(-21.2890327311311,25.8468787778165,-30.6594514707787));
#26711=CARTESIAN_POINT('Ctrl Pts',(-21.2585147040126,25.8161028858665,-30.6621644779852));
#26712=CARTESIAN_POINT('Ctrl Pts',(-21.255179510802,25.812724615011,-30.6624610609334));
#26713=CARTESIAN_POINT('Ctrl Pts',(-21.2501666828563,25.8076245500372,-30.6629069451011));
#26714=CARTESIAN_POINT('Ctrl Pts',(-21.2484835085805,25.8059082469019,-30.6630566811204));
#26715=CARTESIAN_POINT('Ctrl Pts',(-21.245570936239,25.8029316934211,-30.6633158170107));
#26716=CARTESIAN_POINT('Ctrl Pts',(-21.2443406507547,25.8016723191805,-30.6634252872606));
#26717=CARTESIAN_POINT('Ctrl Pts',(-21.2418053389746,25.7990728046313,-30.663650897408));
#26718=CARTESIAN_POINT('Ctrl Pts',(-21.2405004489038,25.7977325377478,-30.6637670262256));
#26719=CARTESIAN_POINT('Ctrl Pts',(-21.2374183707592,25.7945613823296,-30.664041342683));
#26720=CARTESIAN_POINT('Ctrl Pts',(-21.2356421837266,25.7927295126724,-30.6641994509686));
#26721=CARTESIAN_POINT('Ctrl Pts',(-21.2318835565197,25.7888438310577,-30.6645340769204));
#26722=CARTESIAN_POINT('Ctrl Pts',(-21.2299016639369,25.7867894889755,-30.6647105517354));
#26723=CARTESIAN_POINT('Ctrl Pts',(-21.2245417167,25.7812188118585,-30.6651879093344));
#26724=CARTESIAN_POINT('Ctrl Pts',(-21.2211688918846,25.777697421632,-30.6654883892477));
#26725=CARTESIAN_POINT('Ctrl Pts',(-21.1100184276691,25.6611225368121,-30.6753943383473));
#26726=CARTESIAN_POINT('Ctrl Pts',(-21.0105765751098,25.5403720102892,-30.6843764975585));
#26727=CARTESIAN_POINT('Ctrl Pts',(-20.877547983966,25.3525380594509,-30.6973657461954));
#26728=CARTESIAN_POINT('Ctrl Pts',(-20.8369091959534,25.2907556286848,-30.7014960095386));
#26729=CARTESIAN_POINT('Ctrl Pts',(-20.6589738741963,24.9988436939193,-30.7205980272287));
#26730=CARTESIAN_POINT('Ctrl Pts',(-20.548613374255,24.7535998448811,-30.735610210697));
#26731=CARTESIAN_POINT('Ctrl Pts',(-20.4648314815904,24.4811598058575,-30.7528808069889));
#26732=CARTESIAN_POINT('Ctrl Pts',(-20.4599236733617,24.4647354124297,-30.7539236727784));
#26733=CARTESIAN_POINT('Ctrl Pts',(-20.4535215918402,24.4426700812377,-30.7553272176433));
#26734=CARTESIAN_POINT('Ctrl Pts',(-20.4519112059637,24.4370628976378,-30.7556840987633));
#26735=CARTESIAN_POINT('Ctrl Pts',(-20.4494144678361,24.4282797161752,-30.7562434714147));
#26736=CARTESIAN_POINT('Ctrl Pts',(-20.4485177442805,24.4251066586071,-30.7564456243198));
#26737=CARTESIAN_POINT('Ctrl Pts',(-20.4468094100747,24.4190260728576,-30.756833151735));
#26738=CARTESIAN_POINT('Ctrl Pts',(-20.4459970113297,24.4161187679806,-30.7570185003342));
#26739=CARTESIAN_POINT('Ctrl Pts',(-20.4441037279792,24.4093064236934,-30.7574529494429));
#26740=CARTESIAN_POINT('Ctrl Pts',(-20.4430261225694,24.4054004851967,-30.7577021564311));
#26741=CARTESIAN_POINT('Ctrl Pts',(-20.4399504322976,24.3941696247325,-30.7584190316677));
#26742=CARTESIAN_POINT('Ctrl Pts',(-20.4379708730884,24.3868396971216,-30.758887301615));
#26743=CARTESIAN_POINT('Ctrl Pts',(-20.4250967562733,24.338491175706,-30.7619787102857));
#26744=CARTESIAN_POINT('Ctrl Pts',(-20.4149879066645,24.2972694215607,-30.7646272107363));
#26745=CARTESIAN_POINT('Ctrl Pts',(-20.3876267492122,24.175334061134,-30.772503631982));
#26746=CARTESIAN_POINT('Ctrl Pts',(-20.3726584837218,24.0941485426546,-30.7778025121034));
#26747=CARTESIAN_POINT('Ctrl Pts',(-20.3180199506583,23.7171385062734,-30.8026613816379));
#26748=CARTESIAN_POINT('Ctrl Pts',(-20.3164514857571,23.4173368954558,-30.8233146469624));
#26749=CARTESIAN_POINT('Ctrl Pts',(-20.3642743761263,23.0609594223086,-30.8470940150785));
#26750=CARTESIAN_POINT('Ctrl Pts',(-20.3741430726408,23.0005305293944,-30.8510914733854));
#26751=CARTESIAN_POINT('Ctrl Pts',(-20.3865311623377,22.9362470909539,-30.8552819171807));
#26752=CARTESIAN_POINT('Ctrl Pts',(-20.3873427156918,22.9320801605561,-30.8555532656844));
#26753=CARTESIAN_POINT('Ctrl Pts',(-20.38912763034,22.9230110318233,-30.8561432129615));
#26754=CARTESIAN_POINT('Ctrl Pts',(-20.3901041687273,22.918109457786,-30.8564616593882));
#26755=CARTESIAN_POINT('Ctrl Pts',(-20.3929137783052,22.9041763074973,-30.8573656916613));
#26756=CARTESIAN_POINT('Ctrl Pts',(-20.3947742096878,22.895150207601,-30.8579499264987));
#26757=CARTESIAN_POINT('Ctrl Pts',(-20.3996015829667,22.872227401869,-30.8594298547032));
#26758=CARTESIAN_POINT('Ctrl Pts',(-20.4026218030166,22.8583419225298,-30.8603227612037));
#26759=CARTESIAN_POINT('Ctrl Pts',(-20.4065550468342,22.8408177230264,-30.8614447563083));
#26760=CARTESIAN_POINT('Ctrl Pts',(-20.4073826525067,22.8371602887824,-30.861678654897));
#26761=CARTESIAN_POINT('Ctrl Pts',(-20.4087000209977,22.8313852916403,-30.8620475385581));
#26762=CARTESIAN_POINT('Ctrl Pts',(-20.4091855422439,22.8292667800049,-30.8621827677511));
#26763=CARTESIAN_POINT('Ctrl Pts',(-20.4100833454658,22.825367447266,-30.8624314975878));
#26764=CARTESIAN_POINT('Ctrl Pts',(-20.410494996931,22.8235864965073,-30.8625450338012));
#26765=CARTESIAN_POINT('Ctrl Pts',(-20.4114117765175,22.8196355045837,-30.8627967633902));
#26766=CARTESIAN_POINT('Ctrl Pts',(-20.4119176386763,22.8174656418001,-30.8629349133568));
#26767=CARTESIAN_POINT('Ctrl Pts',(-20.4133738798484,22.8112483565606,-30.8633304751454));
#26768=CARTESIAN_POINT('Ctrl Pts',(-20.4143298456853,22.8072022271339,-30.8635875640133));
#26769=CARTESIAN_POINT('Ctrl Pts',(-20.4165018556151,22.798088037533,-30.864165936676));
#26770=CARTESIAN_POINT('Ctrl Pts',(-20.4177223729979,22.7930210401099,-30.8644869657952));
#26771=CARTESIAN_POINT('Ctrl Pts',(-20.4216052914896,22.7770710947,-30.8654959461207));
#26772=CARTESIAN_POINT('Ctrl Pts',(-20.4243121893018,22.7661989159458,-30.8661814234864));
#26773=CARTESIAN_POINT('Ctrl Pts',(-20.4348882757984,22.7246458854925,-30.8687932994691));
#26774=CARTESIAN_POINT('Ctrl Pts',(-20.4431531922583,22.6940664281832,-30.8706987091507));
#26775=CARTESIAN_POINT('Ctrl Pts',(-20.4763521434528,22.5780519023696,-30.8778810748318));
#26776=CARTESIAN_POINT('Ctrl Pts',(-20.5043719285262,22.4935352122634,-30.883017142151));
#26777=CARTESIAN_POINT('Ctrl Pts',(-20.6638256231471,22.0718961832287,-30.9086423038742));
#26778=CARTESIAN_POINT('Ctrl Pts',(-20.8478374017651,21.7575008613413,-30.9281001657211));
#26779=CARTESIAN_POINT('Ctrl Pts',(-21.0933477263073,21.4645502289282,-30.9512144363502));
#26780=CARTESIAN_POINT('Ctrl Pts',(-21.1066246449303,21.4490105086031,-30.9524563951814));
#26781=CARTESIAN_POINT('Ctrl Pts',(-21.1241595226107,21.4288781051536,-30.9540867064273));
#26782=CARTESIAN_POINT('Ctrl Pts',(-21.1282845189385,21.4241698214925,-30.9544695223864));
#26783=CARTESIAN_POINT('Ctrl Pts',(-21.1346599792993,21.4169354833713,-30.9550601177974));
#26784=CARTESIAN_POINT('Ctrl Pts',(-21.136900763485,21.4144008864263,-30.9552674917682));
#26785=CARTESIAN_POINT('Ctrl Pts',(-21.1413635894362,21.4093688821453,-30.9556801054323));
#26786=CARTESIAN_POINT('Ctrl Pts',(-21.1435855342923,21.4068713942104,-30.9558853409126));
#26787=CARTESIAN_POINT('Ctrl Pts',(-21.1485090576894,21.4013546136284,-30.9563396843252));
#26788=CARTESIAN_POINT('Ctrl Pts',(-21.15121244896,21.3983369528698,-30.9565888685124));
#26789=CARTESIAN_POINT('Ctrl Pts',(-21.1589972090813,21.3896801155723,-30.9573056143887));
#26790=CARTESIAN_POINT('Ctrl Pts',(-21.1640927952532,21.3840538118536,-30.9577737774453));
#26791=CARTESIAN_POINT('Ctrl Pts',(-21.1977854299399,21.3471151427167,-30.960862918915));
#26792=CARTESIAN_POINT('Ctrl Pts',(-21.2269771102778,21.3163530579887,-30.9635092164275));
#26793=CARTESIAN_POINT('Ctrl Pts',(-21.3147468184241,21.227443200642,-30.9713833876034));
#26794=CARTESIAN_POINT('Ctrl Pts',(-21.3749576129802,21.1709629224028,-30.9766822698665));
#26795=CARTESIAN_POINT('Ctrl Pts',(-21.5628069315596,21.0078478194128,-30.9929165435534));
#26796=CARTESIAN_POINT('Ctrl Pts',(-21.6965842494174,20.908725455064,-31.0041053059787));
#26797=CARTESIAN_POINT('Ctrl Pts',(-22.0177484779828,20.7072115974436,-31.0297668914548));
#26798=CARTESIAN_POINT('Ctrl Pts',(-22.2088928401764,20.6121876235452,-31.044227353144));
#26799=CARTESIAN_POINT('Ctrl Pts',(-22.4202854353151,20.5320637313955,-31.0584951313363));
#26800=CARTESIAN_POINT('Ctrl Pts',(-22.4325671010641,20.5274940952138,-31.0593180401287));
#26801=CARTESIAN_POINT('Ctrl Pts',(-22.4482929948901,20.5217519175124,-31.0603637199532));
#26802=CARTESIAN_POINT('Ctrl Pts',(-22.4517115739019,20.5205102068063,-31.0605905539662));
#26803=CARTESIAN_POINT('Ctrl Pts',(-22.4571516406263,20.5185446607647,-31.0609507467402));
#26804=CARTESIAN_POINT('Ctrl Pts',(-22.4591717493049,20.5178170585019,-31.061084330922));
#26805=CARTESIAN_POINT('Ctrl Pts',(-22.4629376066325,20.516464923129,-31.0613330389747));
#26806=CARTESIAN_POINT('Ctrl Pts',(-22.4646831553819,20.5158398818747,-31.0614481927496));
#26807=CARTESIAN_POINT('Ctrl Pts',(-22.4685693130123,20.5144521198096,-31.0617042800127));
#26808=CARTESIAN_POINT('Ctrl Pts',(-22.4707101848415,20.513690158252,-31.0618451673615));
#26809=CARTESIAN_POINT('Ctrl Pts',(-22.4769689536497,20.511470044118,-31.0622564959152));
#26810=CARTESIAN_POINT('Ctrl Pts',(-22.4810890325076,20.5100179916889,-31.0625265724818));
#26811=CARTESIAN_POINT('Ctrl Pts',(-22.4904360282522,20.5067451508924,-31.0631377296184));
#26812=CARTESIAN_POINT('Ctrl Pts',(-22.4956647253006,20.5049294359247,-31.0634785128338));
#26813=CARTESIAN_POINT('Ctrl Pts',(-22.5123915937022,20.4991691172093,-31.0645652697315));
#26814=CARTESIAN_POINT('Ctrl Pts',(-22.5239075780579,20.4952760382373,-31.0653083063372));
#26815=CARTESIAN_POINT('Ctrl Pts',(-22.5690511218993,20.4802989495067,-31.0682019070743));
#26816=CARTESIAN_POINT('Ctrl Pts',(-22.6028397255656,20.4697038130985,-31.070326222368));
#26817=CARTESIAN_POINT('Ctrl Pts',(-22.7431133018594,20.4282444850772,-31.0790012601664));
#26818=CARTESIAN_POINT('Ctrl Pts',(-22.8509892320622,20.4023257435799,-31.0853339075474));
#26819=CARTESIAN_POINT('Ctrl Pts',(-23.1894211283398,20.339274232726,-31.1047429962862));
#26820=CARTESIAN_POINT('Ctrl Pts',(-23.4228011284631,20.3215785353226,-31.1175322274701));
#26821=CARTESIAN_POINT('Ctrl Pts',(-23.6977092200726,20.3306078702418,-31.1334451469605));
#26822=CARTESIAN_POINT('Ctrl Pts',(-23.7393402189706,20.3327844487018,-31.1358759734865));
#26823=CARTESIAN_POINT('Ctrl Pts',(-23.7923435688999,20.3365878399093,-31.1390037574374));
#26824=CARTESIAN_POINT('Ctrl Pts',(-23.803766462553,20.3374687693223,-31.1396797831305));
#26825=CARTESIAN_POINT('Ctrl Pts',(-23.8257221586846,20.3392798054361,-31.1409830735552));
#26826=CARTESIAN_POINT('Ctrl Pts',(-23.8362555695916,20.340200877478,-31.1416100723895));
#26827=CARTESIAN_POINT('Ctrl Pts',(-23.8995834695129,20.3460526272284,-31.1453904816775));
#26828=CARTESIAN_POINT('Ctrl Pts',(-23.9522517610108,20.3522335748746,-31.1485800592518));
#26829=CARTESIAN_POINT('Ctrl Pts',(-24.0133907474882,20.3609427497327,-31.152343516821));
#26830=CARTESIAN_POINT('Ctrl Pts',(-24.0220350087488,20.3622099999483,-31.1528770400366));
#26831=CARTESIAN_POINT('Ctrl Pts',(-24.0349149274915,20.3641517298804,-31.1536741395037));
#26832=CARTESIAN_POINT('Ctrl Pts',(-24.039154614404,20.3647995481361,-31.1539368689923));
#26833=CARTESIAN_POINT('Ctrl Pts',(-24.0467160222195,20.3659703720155,-31.1544060681523));
#26834=CARTESIAN_POINT('Ctrl Pts',(-24.0500382476838,20.3664901178466,-31.1546124339637));
#26835=CARTESIAN_POINT('Ctrl Pts',(-24.0570426464262,20.3675971552116,-31.1550479818217));
#26836=CARTESIAN_POINT('Ctrl Pts',(-24.0607246238067,20.3681856391177,-31.1552772015041));
#26837=CARTESIAN_POINT('Ctrl Pts',(-24.0704516824326,20.3697576147968,-31.1558834641308));
#26838=CARTESIAN_POINT('Ctrl Pts',(-24.0764949742184,20.3707519476879,-31.1562608515199));
#26839=CARTESIAN_POINT('Ctrl Pts',(-24.1038653751817,20.3753355074606,-31.1579733744937));
#26840=CARTESIAN_POINT('Ctrl Pts',(-24.1251584599197,20.379122066354,-31.1593147809428));
#26841=CARTESIAN_POINT('Ctrl Pts',(-24.281225190003,20.4084990001218,-31.1692155659));
#26842=CARTESIAN_POINT('Ctrl Pts',(-24.414262639076,20.4424536514726,-31.1780434244342));
#26843=CARTESIAN_POINT('Ctrl Pts',(-24.6778484949909,20.5279630428011,-31.1963246044052));
#26844=CARTESIAN_POINT('Ctrl Pts',(-24.8080148772339,20.5797752720373,-31.2057678805051));
#26845=CARTESIAN_POINT('Ctrl Pts',(-24.996123189273,20.6692373938036,-31.2198674738231));
#26846=CARTESIAN_POINT('Ctrl Pts',(-25.05690510107,20.7005528205261,-31.2244963167398));
#26847=CARTESIAN_POINT('Ctrl Pts',(-25.2073646350865,20.7842314678988,-31.2360817681565));
#26848=CARTESIAN_POINT('Ctrl Pts',(-25.2956007694072,20.8390431807035,-31.2429954405808));
#26849=CARTESIAN_POINT('Ctrl Pts',(-25.4187194192767,20.9240299779544,-31.2526681127528));
#26850=CARTESIAN_POINT('Ctrl Pts',(-25.4558394432219,20.950838660306,-31.2555876826491));
#26851=CARTESIAN_POINT('Ctrl Pts',(-25.4963522876585,20.9814321592773,-31.258766466337));
#26852=CARTESIAN_POINT('Ctrl Pts',(-25.5003197417942,20.9844426706967,-31.2590776837455));
#26853=CARTESIAN_POINT('Ctrl Pts',(-25.5062386342304,20.9889555957295,-31.2595418320974));
#26854=CARTESIAN_POINT('Ctrl Pts',(-25.508195331449,20.9904510510155,-31.2596952488355));
#26855=CARTESIAN_POINT('Ctrl Pts',(-25.5115601203913,20.9930287911824,-31.2599590246219));
#26856=CARTESIAN_POINT('Ctrl Pts',(-25.512969031341,20.994109996825,-31.2600694601017));
#26857=CARTESIAN_POINT('Ctrl Pts',(-25.5157939672834,20.9962815801149,-31.2602908608919));
#26858=CARTESIAN_POINT('Ctrl Pts',(-25.5172099761744,20.9973719688506,-31.2604018245894));
#26859=CARTESIAN_POINT('Ctrl Pts',(-25.5205647300228,20.9999597241063,-31.2606646834562));
#26860=CARTESIAN_POINT('Ctrl Pts',(-25.5225026810649,21.0014581281143,-31.2608165045997));
#26861=CARTESIAN_POINT('Ctrl Pts',(-25.5285788433304,21.0061672342897,-31.2612924446229));
#26862=CARTESIAN_POINT('Ctrl Pts',(-25.5327109638382,21.0093858367416,-31.2616160032855));
#26863=CARTESIAN_POINT('Ctrl Pts',(-25.5422877550396,21.0168830005951,-31.262365698121));
#26864=CARTESIAN_POINT('Ctrl Pts',(-25.547726543163,21.0211690835444,-31.2627913094226));
#26865=CARTESIAN_POINT('Ctrl Pts',(-25.5660502501383,21.0357052161835,-31.2642248797058));
#26866=CARTESIAN_POINT('Ctrl Pts',(-25.5788706710938,21.0460366636189,-31.2652273123123));
#26867=CARTESIAN_POINT('Ctrl Pts',(-25.6319483017241,21.0894848540732,-31.2693777004017));
#26868=CARTESIAN_POINT('Ctrl Pts',(-25.6714804064031,21.1234794045677,-31.2724694932406));
#26869=CARTESIAN_POINT('Ctrl Pts',(-25.7477148101706,21.1923221139306,-31.2784727668281));
#26870=CARTESIAN_POINT('Ctrl Pts',(-25.784455094727,21.2271047441308,-31.2813860179371));
#26871=CARTESIAN_POINT('Ctrl Pts',(-26.0323249684477,21.4730888533598,-31.3013051740137));
#26872=CARTESIAN_POINT('Ctrl Pts',(-26.2140185972063,21.7118690631205,-31.3174240420115));
#26873=CARTESIAN_POINT('Ctrl Pts',(-26.3706122565698,21.9907215525603,-31.3361418853286));
#26874=CARTESIAN_POINT('Ctrl Pts',(-26.3807970178109,22.0092840906525,-31.3373865927799));
#26875=CARTESIAN_POINT('Ctrl Pts',(-26.3934396085583,22.0328745025783,-31.3389675424852));
#26876=CARTESIAN_POINT('Ctrl Pts',(-26.39606839776,22.0378105019966,-31.3392982867036));
#26877=CARTESIAN_POINT('Ctrl Pts',(-26.4005547620264,22.0462875229302,-31.3398662341788));
#26878=CARTESIAN_POINT('Ctrl Pts',(-26.4024186242787,22.0498252152498,-31.3401032338228));
#26879=CARTESIAN_POINT('Ctrl Pts',(-26.4069810209009,22.0585240640669,-31.3406859521046));
#26880=CARTESIAN_POINT('Ctrl Pts',(-26.4096721510493,22.0636890712292,-31.341031909874));
#26881=CARTESIAN_POINT('Ctrl Pts',(-26.4155028921337,22.074954255483,-31.3417864096778));
#26882=CARTESIAN_POINT('Ctrl Pts',(-26.4186370490116,22.0810572105897,-31.3421951281142));
#26883=CARTESIAN_POINT('Ctrl Pts',(-26.4275684606248,22.098586325928,-31.3433690117569));
#26884=CARTESIAN_POINT('Ctrl Pts',(-26.4333170482685,22.1100370220811,-31.3441357760886));
#26885=CARTESIAN_POINT('Ctrl Pts',(-26.4442730895558,22.13218899199,-31.3456191995758));
#26886=CARTESIAN_POINT('Ctrl Pts',(-26.4494898562437,22.1428854430591,-31.3463355301751));
#26887=CARTESIAN_POINT('Ctrl Pts',(-26.4567367310608,22.1579557210437,-31.347344925897));
#26888=CARTESIAN_POINT('Ctrl Pts',(-26.4588164938705,22.1623056711631,-31.3476363001456));
#26889=CARTESIAN_POINT('Ctrl Pts',(-26.46932465279,22.1844114638629,-31.3491171350276));
#26890=CARTESIAN_POINT('Ctrl Pts',(-26.4776001108408,22.2022391805111,-31.3503117667081));
#26891=CARTESIAN_POINT('Ctrl Pts',(-26.4882558587278,22.225755643396,-31.351888476839));
#26892=CARTESIAN_POINT('Ctrl Pts',(-26.4907837513214,22.2313773661323,-31.3522654619498));
#26893=CARTESIAN_POINT('Ctrl Pts',(-26.4946662090913,22.240078125747,-31.3528490358458));
#26894=CARTESIAN_POINT('Ctrl Pts',(-26.4960321172405,22.2431521105773,-31.3530552346233));
#26895=CARTESIAN_POINT('Ctrl Pts',(-26.4987464359722,22.2492865660927,-31.3534667713633));
#26896=CARTESIAN_POINT('Ctrl Pts',(-26.5000949003736,22.2523470085423,-31.3536721071679));
#26897=CARTESIAN_POINT('Ctrl Pts',(-26.5030791519212,22.2591486683573,-31.3541285072096));
#26898=CARTESIAN_POINT('Ctrl Pts',(-26.5047125956162,22.2628909020463,-31.3543796513159));
#26899=CARTESIAN_POINT('Ctrl Pts',(-26.5094216332757,22.2737355149928,-31.3551075499871));
#26900=CARTESIAN_POINT('Ctrl Pts',(-26.5124787434192,22.2808458456486,-31.3555849354727));
#26901=CARTESIAN_POINT('Ctrl Pts',(-26.5333507493752,22.3298766531758,-31.3588778662293));
#26902=CARTESIAN_POINT('Ctrl Pts',(-26.5503000239454,22.37215789966,-31.3617227125035));
#26903=CARTESIAN_POINT('Ctrl Pts',(-26.5971043802589,22.4964820530526,-31.3701083297386));
#26904=CARTESIAN_POINT('Ctrl Pts',(-26.6245270168094,22.5793907976896,-31.3757273694872));
#26905=CARTESIAN_POINT('Ctrl Pts',(-26.7312608791712,22.9522346532994,-31.4011103371355));
#26906=CARTESIAN_POINT('Ctrl Pts',(-26.773135959949,23.251247164315,-31.4219442594993));
#26907=CARTESIAN_POINT('Ctrl Pts',(-26.7730022123545,23.5516872106683,-31.4417267961338));
#26908=CARTESIAN_POINT('Ctrl Pts',(-26.7730022103292,23.5516917530075,-31.4417270952249));
#26909=CARTESIAN_POINT('Ctrl Pts',(-26.7729671701148,23.6301549043037,-31.4468935140642));
#26910=CARTESIAN_POINT('Ctrl Pts',(-26.7700666504897,23.7085998482106,-31.4519687193417));
#26911=CARTESIAN_POINT('Ctrl Pts',(-26.7639460041217,23.7917389120325,-31.4571986492526));
#26912=CARTESIAN_POINT('Ctrl Pts',(-26.763576417344,23.7966079928911,-31.4575043968517));
#26913=CARTESIAN_POINT('Ctrl Pts',(-26.7629730222354,23.8043249163732,-31.4579880854355));
#26914=CARTESIAN_POINT('Ctrl Pts',(-26.7627464924713,23.8071732959786,-31.4581664275246));
#26915=CARTESIAN_POINT('Ctrl Pts',(-26.7623537222974,23.8120302345219,-31.4584701983748));
#26916=CARTESIAN_POINT('Ctrl Pts',(-26.76218938594,23.8140389391592,-31.4585957336956));
#26917=CARTESIAN_POINT('Ctrl Pts',(-26.7618790954275,23.817788377989,-31.45882987556));
#26918=CARTESIAN_POINT('Ctrl Pts',(-26.7617336101885,23.819529148648,-31.4589385086088));
#26919=CARTESIAN_POINT('Ctrl Pts',(-26.7614280364084,23.823149949312,-31.4591643117892));
#26920=CARTESIAN_POINT('Ctrl Pts',(-26.761267712553,23.8250299523968,-31.4592814677161));
#26921=CARTESIAN_POINT('Ctrl Pts',(-26.7608950755778,23.8293547350151,-31.4595507778698));
#26922=CARTESIAN_POINT('Ctrl Pts',(-26.760681620535,23.8317994196452,-31.4597028671405));
#26923=CARTESIAN_POINT('Ctrl Pts',(-26.7599946254918,23.8395651505979,-31.4601855378776));
#26924=CARTESIAN_POINT('Ctrl Pts',(-26.7595106442483,23.8448852999507,-31.4605155308063));
#26925=CARTESIAN_POINT('Ctrl Pts',(-26.7552520026556,23.8904425048174,-31.463335710523));
#26926=CARTESIAN_POINT('Ctrl Pts',(-26.7507338025173,23.9306087227669,-31.4657847612494));
#26927=CARTESIAN_POINT('Ctrl Pts',(-26.744956905583,23.9745124232755,-31.4684310361837));
#26928=CARTESIAN_POINT('Ctrl Pts',(-26.7444459440973,23.9783424014542,-31.4686616299177));
#26929=CARTESIAN_POINT('Ctrl Pts',(-26.7426260008648,23.9917993437584,-31.4694709675826));
#26930=CARTESIAN_POINT('Ctrl Pts',(-26.7412803627848,24.001421390797,-31.4700480944473));
#26931=CARTESIAN_POINT('Ctrl Pts',(-26.739568855722,24.0132687636727,-31.4707569216899));
#26932=CARTESIAN_POINT('Ctrl Pts',(-26.7392441515003,24.0154998794983,-31.4708903315642));
#26933=CARTESIAN_POINT('Ctrl Pts',(-26.7378330467221,24.0251250139474,-31.4714655400248));
#26934=CARTESIAN_POINT('Ctrl Pts',(-26.736723261678,24.0325156372822,-31.4719063769354));
#26935=CARTESIAN_POINT('Ctrl Pts',(-26.7340278152987,24.0500504125977,-31.4729504517365));
#26936=CARTESIAN_POINT('Ctrl Pts',(-26.7324193588308,24.060191024947,-31.473552790028));
#26937=CARTESIAN_POINT('Ctrl Pts',(-26.7287638285546,24.0825465157908,-31.474877777624));
#26938=CARTESIAN_POINT('Ctrl Pts',(-26.726694741267,24.0947576704901,-31.4755996082634));
#26939=CARTESIAN_POINT('Ctrl Pts',(-26.6708967325278,24.4129154496872,-31.4943637072343));
#26940=CARTESIAN_POINT('Ctrl Pts',(-26.5732867784656,24.7095217629079,-31.5109806629215));
#26941=CARTESIAN_POINT('Ctrl Pts',(-26.3998230380398,25.0576306333022,-31.5334894702754));
#26942=CARTESIAN_POINT('Ctrl Pts',(-26.3623861692889,25.1263692166543,-31.5380859597871));
#26943=CARTESIAN_POINT('Ctrl Pts',(-26.302231018629,25.2278430109924,-31.5451480538195));
#26944=CARTESIAN_POINT('Ctrl Pts',(-26.2813457101815,25.2616336242055,-31.547547838486));
#26945=CARTESIAN_POINT('Ctrl Pts',(-26.2558069777853,25.3012945775034,-31.5504254386768));
#26946=CARTESIAN_POINT('Ctrl Pts',(-26.2517503749817,25.3075466186917,-31.5508808803033));
#26947=CARTESIAN_POINT('Ctrl Pts',(-26.2454713079989,25.3171507987376,-31.5515833526639));
#26948=CARTESIAN_POINT('Ctrl Pts',(-26.2432641755925,25.3205129712401,-31.5518298078829));
#26949=CARTESIAN_POINT('Ctrl Pts',(-26.2392290095888,25.3266348163798,-31.552279539537));
#26950=CARTESIAN_POINT('Ctrl Pts',(-26.2374030043203,25.3293958247852,-31.5524827394345));
#26951=CARTESIAN_POINT('Ctrl Pts',(-26.2336966534207,25.334981284565,-31.5528945542364));
#26952=CARTESIAN_POINT('Ctrl Pts',(-26.2318160948289,25.3378055889431,-31.5531031770062));
#26953=CARTESIAN_POINT('Ctrl Pts',(-26.2264259250756,25.3458731319475,-31.5537002141623));
#26954=CARTESIAN_POINT('Ctrl Pts',(-26.2229053862977,25.3511090194161,-31.5540890415846));
#26955=CARTESIAN_POINT('Ctrl Pts',(-26.2076811182781,25.373608193274,-31.5557657151199));
#26956=CARTESIAN_POINT('Ctrl Pts',(-26.1958255408818,25.3907676719544,-31.5570593220089));
#26957=CARTESIAN_POINT('Ctrl Pts',(-25.9783852742474,25.6990434990484,-31.5805739475404));
#26958=CARTESIAN_POINT('Ctrl Pts',(-25.7261111862444,25.9541309542022,-31.6049071370198));
#26959=CARTESIAN_POINT('Ctrl Pts',(-25.3912798682883,26.1959979080524,-31.6326461065456));
#26960=CARTESIAN_POINT('Ctrl Pts',(-25.3443152646014,26.2280668805358,-31.636439443643));
#26961=CARTESIAN_POINT('Ctrl Pts',(-25.2482199101226,26.2900203305189,-31.6439750669341));
#26962=CARTESIAN_POINT('Ctrl Pts',(-25.1990870411787,26.3198673881172,-31.6477150910901));
#26963=CARTESIAN_POINT('Ctrl Pts',(-25.1334960367396,26.3573477978747,-31.6525365582984));
#26964=CARTESIAN_POINT('Ctrl Pts',(-25.1177375760591,26.3661776904649,-31.6536822439895));
#26965=CARTESIAN_POINT('Ctrl Pts',(-25.0954066340541,26.3784447704623,-31.6552870626515));
#26966=CARTESIAN_POINT('Ctrl Pts',(-25.088895592973,26.3819922923328,-31.6557527560709));
#26967=CARTESIAN_POINT('Ctrl Pts',(-25.0775080763461,26.3881458759834,-31.6565632799256));
#26968=CARTESIAN_POINT('Ctrl Pts',(-25.0726370612939,26.3907619010414,-31.6569087251532));
#26969=CARTESIAN_POINT('Ctrl Pts',(-25.0655463515619,26.3945465555632,-31.6574097366201));
#26970=CARTESIAN_POINT('Ctrl Pts',(-25.0633320207231,26.3957251312335,-31.6575659338356));
#26971=CARTESIAN_POINT('Ctrl Pts',(-25.0595494071545,26.3977327600747,-31.6578323069753));
#26972=CARTESIAN_POINT('Ctrl Pts',(-25.057981814435,26.3985631045279,-31.6579425658475));
#26973=CARTESIAN_POINT('Ctrl Pts',(-25.0548613333531,26.4002127066934,-31.6581617864368));
#26974=CARTESIAN_POINT('Ctrl Pts',(-25.0533084629692,26.4010319887212,-31.6582707497144));
#26975=CARTESIAN_POINT('Ctrl Pts',(-25.0496445403041,26.4029612191554,-31.65852754045));
#26976=CARTESIAN_POINT('Ctrl Pts',(-25.0475329203326,26.404070095745,-31.6586752991903));
#26977=CARTESIAN_POINT('Ctrl Pts',(-25.0412799644029,26.4073448646553,-31.6591121494404));
#26978=CARTESIAN_POINT('Ctrl Pts',(-25.0371351231144,26.4095041058193,-31.6594008195763));
#26979=CARTESIAN_POINT('Ctrl Pts',(-25.0005370548299,26.4284686443872,-31.6619419082835));
#26980=CARTESIAN_POINT('Ctrl Pts',(-24.9678031840086,26.4447306564743,-31.6641606311909));
#26981=CARTESIAN_POINT('Ctrl Pts',(-24.9250026665692,26.4650934017123,-31.667001268736));
#26982=CARTESIAN_POINT('Ctrl Pts',(-24.9151836461309,26.4697042422017,-31.6676488799276));
#26983=CARTESIAN_POINT('Ctrl Pts',(-24.9041223353676,26.4748304367094,-31.6683740683415));
#26984=CARTESIAN_POINT('Ctrl Pts',(-24.902902913269,26.4753946330368,-31.6684539552863));
#26985=CARTESIAN_POINT('Ctrl Pts',(-24.8949734676219,26.4790573719504,-31.668973046763));
#26986=CARTESIAN_POINT('Ctrl Pts',(-24.888253100853,26.4821336115829,-31.6694112031724));
#26987=CARTESIAN_POINT('Ctrl Pts',(-24.8779851799299,26.4867910826827,-31.6700780242888));
#26988=CARTESIAN_POINT('Ctrl Pts',(-24.8744452929799,26.4883890461963,-31.6703074369775));
#26989=CARTESIAN_POINT('Ctrl Pts',(-24.8674443493263,26.4915341656879,-31.6707602315558));
#26990=CARTESIAN_POINT('Ctrl Pts',(-24.8639834350638,26.4930816209663,-31.670983626237));
#26991=CARTESIAN_POINT('Ctrl Pts',(-24.7185394613715,26.5578052961059,-31.6803534140283));
#26992=CARTESIAN_POINT('Ctrl Pts',(-24.5721613300134,26.6106412801705,-31.6890580758463));
#26993=CARTESIAN_POINT('Ctrl Pts',(-24.4056671135617,26.657452284008,-31.6987258234761));
#26994=CARTESIAN_POINT('Ctrl Pts',(-24.3887655649884,26.6620559158255,-31.6997045351701));
#26995=CARTESIAN_POINT('Ctrl Pts',(-24.3523996410172,26.6716434469892,-31.7018059127665));
#26996=CARTESIAN_POINT('Ctrl Pts',(-24.3329245163827,26.6765835752178,-31.7029285479905));
#26997=CARTESIAN_POINT('Ctrl Pts',(-24.2906526495927,26.686886655365,-31.7053613799287));
#26998=CARTESIAN_POINT('Ctrl Pts',(-24.2678411222388,26.6921838751518,-31.7066717832037));
#26999=CARTESIAN_POINT('Ctrl Pts',(-24.2176883076366,26.7032555190323,-31.7095504538854));
#27000=CARTESIAN_POINT('Ctrl Pts',(-24.190325665609,26.7089238841405,-31.7111194988788));
#27001=CARTESIAN_POINT('Ctrl Pts',(-24.0695755187937,26.7323046739457,-31.7180466004763));
#27002=CARTESIAN_POINT('Ctrl Pts',(-23.9755090541764,26.7462355450478,-31.7234524754065));
#27003=CARTESIAN_POINT('Ctrl Pts',(-23.7841016460363,26.7659818857433,-31.7346167739771));
#27004=CARTESIAN_POINT('Ctrl Pts',(-23.6868396602599,26.771578627305,-31.7403748797362));
#27005=CARTESIAN_POINT('Ctrl Pts',(-23.5719807043389,26.7729768019354,-31.7473348747763));
#27006=CARTESIAN_POINT('Ctrl Pts',(-23.5544801755576,26.7730472728566,-31.7483996454995));
#27007=CARTESIAN_POINT('Ctrl Pts',(-23.5313158936095,26.7729518740491,-31.7498149800078));
#27008=CARTESIAN_POINT('Ctrl Pts',(-23.5256516816213,26.7729136130064,-31.7501615347802));
#27009=CARTESIAN_POINT('Ctrl Pts',(-23.516361776207,26.7728263674901,-31.7507307057313));
#27010=CARTESIAN_POINT('Ctrl Pts',(-23.5127359959132,26.7727861963494,-31.7509530448978));
#27011=CARTESIAN_POINT('Ctrl Pts',(-23.5057173616474,26.7726965878503,-31.7513838222347));
#27012=CARTESIAN_POINT('Ctrl Pts',(-23.5023245013513,26.7726479109414,-31.7515922362406));
#27013=CARTESIAN_POINT('Ctrl Pts',(-23.4945014558309,26.7725233167755,-31.7520731860221));
#27014=CARTESIAN_POINT('Ctrl Pts',(-23.4900713451068,26.7724436215143,-31.752345840088));
#27015=CARTESIAN_POINT('Ctrl Pts',(-23.4762851409093,26.7721671741008,-31.7531952538741));
#27016=CARTESIAN_POINT('Ctrl Pts',(-23.4669297932438,26.7719388069461,-31.7537730052068));
#27017=CARTESIAN_POINT('Ctrl Pts',(-23.3875781151358,26.7696559402467,-31.7586850076445));
#27018=CARTESIAN_POINT('Ctrl Pts',(-23.3176696867381,26.7653614335192,-31.7630892655988));
#27019=CARTESIAN_POINT('Ctrl Pts',(-23.2394771357738,26.7579945454056,-31.7681075218243));
#27020=CARTESIAN_POINT('Ctrl Pts',(-23.2309967787604,26.7571616253986,-31.7686529859288));
#27021=CARTESIAN_POINT('Ctrl Pts',(-23.167436973454,26.7506643245458,-31.7727502982384));
#27022=CARTESIAN_POINT('Ctrl Pts',(-23.1125110255552,26.7436152119414,-31.7763424882658));
#27023=CARTESIAN_POINT('Ctrl Pts',(-22.8633872303512,26.7050951771669,-31.7928643244734));
#27024=CARTESIAN_POINT('Ctrl Pts',(-22.6721543961242,26.6573002418126,-31.8062188117439));
#27025=CARTESIAN_POINT('Ctrl Pts',(-22.3835125292605,26.5563691939994,-31.8268870325203));
#27026=CARTESIAN_POINT('Ctrl Pts',(-22.2824186403182,26.5151504775598,-31.8342215566646));
#27027=CARTESIAN_POINT('Ctrl Pts',(-22.147086342378,26.4517811304981,-31.8440175553199));
#27028=CARTESIAN_POINT('Ctrl Pts',(-22.1108903054392,26.4339966676922,-31.8466349789575));
#27029=CARTESIAN_POINT('Ctrl Pts',(-22.0750360153402,26.4155367745532,-31.8492183260801));
#27030=CARTESIAN_POINT('Ctrl Pts',(-22.0750360188393,26.4155367763548,-32.0936416103654));
#27031=CARTESIAN_POINT('Ctrl Pts',(-22.099508153078,26.4281364675027,-32.0917876278781));
#27032=CARTESIAN_POINT('Ctrl Pts',(-22.1241485350163,26.4404261539109,-32.0899290872953));
#27033=CARTESIAN_POINT('Ctrl Pts',(-22.3021405079941,26.5263694585511,-32.0765701184169));
#27034=CARTESIAN_POINT('Ctrl Pts',(-22.4609515178144,26.5880945217143,-32.0649839042452));
#27035=CARTESIAN_POINT('Ctrl Pts',(-22.672592506279,26.6516095084807,-32.0504662776571));
#27036=CARTESIAN_POINT('Ctrl Pts',(-22.7216285051253,26.6650695515949,-32.0471658601115));
#27037=CARTESIAN_POINT('Ctrl Pts',(-22.7971629712594,26.6838930052114,-32.0421987407113));
#27038=CARTESIAN_POINT('Ctrl Pts',(-22.8234427352679,26.6900923589496,-32.0404919919648));
#27039=CARTESIAN_POINT('Ctrl Pts',(-22.8540807623507,26.6969145215607,-32.0385294665726));
#27040=CARTESIAN_POINT('Ctrl Pts',(-22.8583651546385,26.6978593478192,-32.0382556466428));
#27041=CARTESIAN_POINT('Ctrl Pts',(-22.8648880253284,26.6992838583967,-32.0378397169844));
#27042=CARTESIAN_POINT('Ctrl Pts',(-22.8671250856603,26.6997699067365,-32.0376972417929));
#27043=CARTESIAN_POINT('Ctrl Pts',(-22.8711853150902,26.7006475474158,-32.0374389633542));
#27044=CARTESIAN_POINT('Ctrl Pts',(-22.8730083001809,26.7010399397377,-32.0373231141769));
#27045=CARTESIAN_POINT('Ctrl Pts',(-22.8769584286894,26.7018866069624,-32.0370723342303));
#27046=CARTESIAN_POINT('Ctrl Pts',(-22.8790856858302,26.7023403094398,-32.0369374370961));
#27047=CARTESIAN_POINT('Ctrl Pts',(-22.8848882932016,26.7035717520788,-32.0365698912813));
#27048=CARTESIAN_POINT('Ctrl Pts',(-22.8885645612441,26.7043452230422,-32.0363374888414));
#27049=CARTESIAN_POINT('Ctrl Pts',(-22.9062194276443,26.7080275054709,-32.0352235627163));
#27050=CARTESIAN_POINT('Ctrl Pts',(-22.9202161845924,26.7108498871461,-32.0343469421178));
#27051=CARTESIAN_POINT('Ctrl Pts',(-22.9432036681648,26.7153264315599,-32.0329171872676));
#27052=CARTESIAN_POINT('Ctrl Pts',(-22.9521833053234,26.7170354922394,-32.0323611644874));
#27053=CARTESIAN_POINT('Ctrl Pts',(-22.9661359248567,26.7196295781824,-32.0315008964205));
#27054=CARTESIAN_POINT('Ctrl Pts',(-22.9711038374556,26.7205411406121,-32.0311953167347));
#27055=CARTESIAN_POINT('Ctrl Pts',(-22.9811219353428,26.722355027642,-32.0305805178028));
#27056=CARTESIAN_POINT('Ctrl Pts',(-22.9861721747632,26.7232569805009,-32.0302713175148));
#27057=CARTESIAN_POINT('Ctrl Pts',(-23.3006925612394,26.7786544411731,-32.0110588758788));
#27058=CARTESIAN_POINT('Ctrl Pts',(-23.6165153703464,26.7876180436505,-31.9942836676612));
#27059=CARTESIAN_POINT('Ctrl Pts',(-24.0051908355359,26.7416604620454,-31.9720327086367));
#27060=CARTESIAN_POINT('Ctrl Pts',(-24.0813495013313,26.7298733216919,-31.9676034726495));
#27061=CARTESIAN_POINT('Ctrl Pts',(-24.2364518921627,26.7001399949314,-31.9583694496124));
#27062=CARTESIAN_POINT('Ctrl Pts',(-24.3152870336579,26.6819263847318,-31.9535602268042));
#27063=CARTESIAN_POINT('Ctrl Pts',(-24.4083988206492,26.6566886966496,-31.9477081244511));
#27064=CARTESIAN_POINT('Ctrl Pts',(-24.4234186455926,26.6525003658251,-31.9467587520726));
#27065=CARTESIAN_POINT('Ctrl Pts',(-24.4423168605814,26.6470824167095,-31.9455572709253));
#27066=CARTESIAN_POINT('Ctrl Pts',(-24.4462243005283,26.645954179594,-31.9453084733732));
#27067=CARTESIAN_POINT('Ctrl Pts',(-24.4532285327579,26.643917400355,-31.9448618148281));
#27068=CARTESIAN_POINT('Ctrl Pts',(-24.4563261209214,26.6430115958419,-31.9446640434848));
#27069=CARTESIAN_POINT('Ctrl Pts',(-24.4625755027005,26.6411739414436,-31.9442645556436));
#27070=CARTESIAN_POINT('Ctrl Pts',(-24.4657272415048,26.6402419200644,-31.9440628337363));
#27071=CARTESIAN_POINT('Ctrl Pts',(-24.4720409092905,26.6383643563047,-31.9436582362708));
#27072=CARTESIAN_POINT('Ctrl Pts',(-24.4752028225904,26.6374187749689,-31.9434553596357));
#27073=CARTESIAN_POINT('Ctrl Pts',(-24.4837471465164,26.6348492596578,-31.9429064477829));
#27074=CARTESIAN_POINT('Ctrl Pts',(-24.4891267509622,26.6332161010247,-31.9425601102259));
#27075=CARTESIAN_POINT('Ctrl Pts',(-24.5102331235181,26.6267481894661,-31.9411983733315));
#27076=CARTESIAN_POINT('Ctrl Pts',(-24.5259268319407,26.6218071726948,-31.9401794866225));
#27077=CARTESIAN_POINT('Ctrl Pts',(-24.7960124758728,26.534494488316,-31.9225326301285));
#27078=CARTESIAN_POINT('Ctrl Pts',(-25.0391605311647,26.4209161073131,-31.9047925280574));
#27079=CARTESIAN_POINT('Ctrl Pts',(-25.3342556629352,26.2354074398297,-31.881212746759));
#27080=CARTESIAN_POINT('Ctrl Pts',(-25.4014077988599,26.1895608608288,-31.8757019961106));
#27081=CARTESIAN_POINT('Ctrl Pts',(-25.5892536727295,26.0506141001433,-31.8599698365334));
#27082=CARTESIAN_POINT('Ctrl Pts',(-25.7051902539378,25.9514168619256,-31.8498567385606));
#27083=CARTESIAN_POINT('Ctrl Pts',(-25.8177666183684,25.8403464848335,-31.8399519287678));
#27084=CARTESIAN_POINT('Ctrl Pts',(-25.8218380447533,25.8363080221709,-31.8395935993931));
#27085=CARTESIAN_POINT('Ctrl Pts',(-25.8277071462057,25.8304552779514,-31.8390769213745));
#27086=CARTESIAN_POINT('Ctrl Pts',(-25.8295134483037,25.8286497225553,-31.8389178877137));
#27087=CARTESIAN_POINT('Ctrl Pts',(-25.8326569320553,25.8255000589626,-31.8386410945821));
#27088=CARTESIAN_POINT('Ctrl Pts',(-25.8339950754361,25.8241569164711,-31.8385232579414));
#27089=CARTESIAN_POINT('Ctrl Pts',(-25.8365871690197,25.8215505431322,-31.838294982161));
#27090=CARTESIAN_POINT('Ctrl Pts',(-25.8378412546809,25.8202874576588,-31.8381845319204));
#27091=CARTESIAN_POINT('Ctrl Pts',(-25.8408383405488,25.8172638576927,-31.837920551206));
#27092=CARTESIAN_POINT('Ctrl Pts',(-25.8425803616032,25.8155023678608,-31.8377670989777));
#27093=CARTESIAN_POINT('Ctrl Pts',(-25.8488228842705,25.8091755037698,-31.8372171365467));
#27094=CARTESIAN_POINT('Ctrl Pts',(-25.8533118314653,25.8045986725801,-31.8368215374142));
#27095=CARTESIAN_POINT('Ctrl Pts',(-25.9204921765884,25.7356929876222,-31.8308986482986));
#27096=CARTESIAN_POINT('Ctrl Pts',(-25.9804878180238,25.6687769911317,-31.825576660699));
#27097=CARTESIAN_POINT('Ctrl Pts',(-26.2272038826552,25.3693051862334,-31.8030981683612));
#27098=CARTESIAN_POINT('Ctrl Pts',(-26.3839477802576,25.1139725137947,-31.787094809092));
#27099=CARTESIAN_POINT('Ctrl Pts',(-26.5364078101719,24.7650802226755,-31.7651202686616));
#27100=CARTESIAN_POINT('Ctrl Pts',(-26.5665370044784,24.6882138758409,-31.7602836583404));
#27101=CARTESIAN_POINT('Ctrl Pts',(-26.6076296514555,24.5702334173207,-31.7528145787027));
#27102=CARTESIAN_POINT('Ctrl Pts',(-26.6207856268887,24.5299168157773,-31.7502546265053));
#27103=CARTESIAN_POINT('Ctrl Pts',(-26.6353538752722,24.4820920501767,-31.7472052100246));
#27104=CARTESIAN_POINT('Ctrl Pts',(-26.6375402435065,24.4748225784133,-31.7467413507094));
#27105=CARTESIAN_POINT('Ctrl Pts',(-26.6408541345635,24.4636613729258,-31.7460286169164));
#27106=CARTESIAN_POINT('Ctrl Pts',(-26.6420000463417,24.459775090144,-31.7457803448455));
#27107=CARTESIAN_POINT('Ctrl Pts',(-26.643986948663,24.4529894994882,-31.7453466723294));
#27108=CARTESIAN_POINT('Ctrl Pts',(-26.6448312017001,24.4500911454493,-31.7451613788289));
#27109=CARTESIAN_POINT('Ctrl Pts',(-26.6465891875138,24.4440241755646,-31.7447733919892));
#27110=CARTESIAN_POINT('Ctrl Pts',(-26.6475021312051,24.4408553364066,-31.7445706731151));
#27111=CARTESIAN_POINT('Ctrl Pts',(-26.6500170264353,24.4320754672165,-31.7440088067331));
#27112=CARTESIAN_POINT('Ctrl Pts',(-26.6516085989866,24.4264614997047,-31.7436493209781));
#27113=CARTESIAN_POINT('Ctrl Pts',(-26.6578179067946,24.4043304783406,-31.7422312874853));
#27114=CARTESIAN_POINT('Ctrl Pts',(-26.6623189449261,24.3877812301906,-31.741168946694));
#27115=CARTESIAN_POINT('Ctrl Pts',(-26.7375347627839,24.1022501202929,-31.7228040984325));
#27116=CARTESIAN_POINT('Ctrl Pts',(-26.7732536883996,23.8253238402451,-31.7042898690192));
#27117=CARTESIAN_POINT('Ctrl Pts',(-26.7729665957051,23.5092218944626,-31.6828951409107));
#27118=CARTESIAN_POINT('Ctrl Pts',(-26.7722562232377,23.4711217833702,-31.6803149608563));
#27119=CARTESIAN_POINT('Ctrl Pts',(-26.7644303207503,23.2560857020112,-31.6657657622672));
#27120=CARTESIAN_POINT('Ctrl Pts',(-26.7434157378901,23.0799352991948,-31.6538820381171));
#27121=CARTESIAN_POINT('Ctrl Pts',(-26.7058780190909,22.8958358037867,-31.6420498464673));
#27122=CARTESIAN_POINT('Ctrl Pts',(-26.7036742033385,22.8852974662144,-31.6413746745486));
#27123=CARTESIAN_POINT('Ctrl Pts',(-26.7007030161701,22.8714367023745,-31.6404896323586));
#27124=CARTESIAN_POINT('Ctrl Pts',(-26.6999831573655,22.8681043284166,-31.6402770805511));
#27125=CARTESIAN_POINT('Ctrl Pts',(-26.6988607096658,22.8629479463126,-31.6399485462579));
#27126=CARTESIAN_POINT('Ctrl Pts',(-26.698461823381,22.8611231481565,-31.6398323506808));
#27127=CARTESIAN_POINT('Ctrl Pts',(-26.697661010985,22.857474851877,-31.6396001833679));
#27128=CARTESIAN_POINT('Ctrl Pts',(-26.6972590890948,22.8556513678103,-31.6394842127192));
#27129=CARTESIAN_POINT('Ctrl Pts',(-26.6963524134703,22.851554801634,-31.6392238358332));
#27130=CARTESIAN_POINT('Ctrl Pts',(-26.6958467820369,22.8492819214714,-31.6390794812575));
#27131=CARTESIAN_POINT('Ctrl Pts',(-26.6943403469148,22.8425447501263,-31.6386519102628));
#27132=CARTESIAN_POINT('Ctrl Pts',(-26.6933324942288,22.8380820158505,-31.6383691000201));
#27133=CARTESIAN_POINT('Ctrl Pts',(-26.6852159230003,22.8024949834775,-31.6361170968028));
#27134=CARTESIAN_POINT('Ctrl Pts',(-26.677654249942,22.7714743239807,-31.6341736065395));
#27135=CARTESIAN_POINT('Ctrl Pts',(-26.6494075755702,22.6626513238917,-31.6274082600648));
#27136=CARTESIAN_POINT('Ctrl Pts',(-26.626268577755,22.5855114800766,-31.6227076184188));
#27137=CARTESIAN_POINT('Ctrl Pts',(-26.4754428656927,22.1435836564873,-31.5959084979339));
#27138=CARTESIAN_POINT('Ctrl Pts',(-26.2858780751226,21.8032999665366,-31.5753607361601));
#27139=CARTESIAN_POINT('Ctrl Pts',(-26.0278316041391,21.4891553492079,-31.550770459468));
#27140=CARTESIAN_POINT('Ctrl Pts',(-26.014959557988,21.4737798248807,-31.5495518380616));
#27141=CARTESIAN_POINT('Ctrl Pts',(-25.9979124874068,21.453799120331,-31.5479479241696));
#27142=CARTESIAN_POINT('Ctrl Pts',(-25.9938662510642,21.4490842484604,-31.5475679472693));
#27143=CARTESIAN_POINT('Ctrl Pts',(-25.9876018397336,21.4418272198131,-31.5469807632382));
#27144=CARTESIAN_POINT('Ctrl Pts',(-25.9853932489911,21.4392767781608,-31.5467739540099));
#27145=CARTESIAN_POINT('Ctrl Pts',(-25.9809878159776,21.4342055755476,-31.5463618491365));
#27146=CARTESIAN_POINT('Ctrl Pts',(-25.9787910473817,21.431684755916,-31.5461565567016));
#27147=CARTESIAN_POINT('Ctrl Pts',(-25.9739136021094,21.426105380699,-31.5457011974784));
#27148=CARTESIAN_POINT('Ctrl Pts',(-25.9712310540105,21.4230484752933,-31.5454510526797));
#27149=CARTESIAN_POINT('Ctrl Pts',(-25.9634774421054,21.4142464886248,-31.5447288893735));
#27150=CARTESIAN_POINT('Ctrl Pts',(-25.958391690382,21.4085144349542,-31.544256255268));
#27151=CARTESIAN_POINT('Ctrl Pts',(-25.9240405623118,21.3700749731657,-31.5410708341378));
#27152=CARTESIAN_POINT('Ctrl Pts',(-25.8941313316755,21.3379515429586,-31.5383308851528));
#27153=CARTESIAN_POINT('Ctrl Pts',(-25.8124474623153,21.2537367921335,-31.5309310567334));
#27154=CARTESIAN_POINT('Ctrl Pts',(-25.7595351166022,21.2027901733812,-31.5262224063497));
#27155=CARTESIAN_POINT('Ctrl Pts',(-25.5931411847298,21.0531897174514,-31.5116626298826));
#27156=CARTESIAN_POINT('Ctrl Pts',(-25.4744656083958,20.9606362568154,-31.501598282119));
#27157=CARTESIAN_POINT('Ctrl Pts',(-25.1540162765927,20.7449462415519,-31.4754912088065));
#27158=CARTESIAN_POINT('Ctrl Pts',(-24.944357773292,20.635069194381,-31.4593569162729));
#27159=CARTESIAN_POINT('Ctrl Pts',(-24.7120466367349,20.5441699177788,-31.443607863754));
#27160=CARTESIAN_POINT('Ctrl Pts',(-24.6994988870679,20.5393504984236,-31.4427636179599));
#27161=CARTESIAN_POINT('Ctrl Pts',(-24.6834846601421,20.5333143499677,-31.4416946078555));
#27162=CARTESIAN_POINT('Ctrl Pts',(-24.6800459954441,20.5320249427118,-31.4414655593854));
#27163=CARTESIAN_POINT('Ctrl Pts',(-24.6745855759095,20.5299880707178,-31.4411026366636));
#27164=CARTESIAN_POINT('Ctrl Pts',(-24.6725652755543,20.5292367565639,-31.4409685312059));
#27165=CARTESIAN_POINT('Ctrl Pts',(-24.6688288471521,20.5278515100017,-31.4407208313979));
#27166=CARTESIAN_POINT('Ctrl Pts',(-24.6671129441123,20.5272170160854,-31.4406072037327));
#27167=CARTESIAN_POINT('Ctrl Pts',(-24.6632865415761,20.5258058198558,-31.4403540960606));
#27168=CARTESIAN_POINT('Ctrl Pts',(-24.6611757737163,20.5250298671101,-31.4402146617738));
#27169=CARTESIAN_POINT('Ctrl Pts',(-24.656778072143,20.5234184234391,-31.4399245441745));
#27170=CARTESIAN_POINT('Ctrl Pts',(-24.6544909991105,20.5225833130157,-31.4397738837476));
#27171=CARTESIAN_POINT('Ctrl Pts',(-24.6485724780854,20.5204298003499,-31.4393845618823));
#27172=CARTESIAN_POINT('Ctrl Pts',(-24.6449395886151,20.5191153299518,-31.4391461337008));
#27173=CARTESIAN_POINT('Ctrl Pts',(-24.6342978316785,20.5152865029144,-31.4384492782468));
#27174=CARTESIAN_POINT('Ctrl Pts',(-24.6272825454265,20.5127898800189,-31.4379918836948));
#27175=CARTESIAN_POINT('Ctrl Pts',(-24.5533416179106,20.4867639152512,-31.4331912368279));
#27176=CARTESIAN_POINT('Ctrl Pts',(-24.4856592661558,20.4654241404961,-31.4289714742513));
#27177=CARTESIAN_POINT('Ctrl Pts',(-24.3413968316429,20.4251248968509,-31.4202339904514));
#27178=CARTESIAN_POINT('Ctrl Pts',(-24.2647146840019,20.4067072037797,-31.4157380672096));
#27179=CARTESIAN_POINT('Ctrl Pts',(-23.8541433891334,20.3238974740217,-31.3920938532711));
#27180=CARTESIAN_POINT('Ctrl Pts',(-23.5123593490702,20.3098401169598,-31.3736219133235));
#27181=CARTESIAN_POINT('Ctrl Pts',(-23.1549569878328,20.3517757514882,-31.3518531529117));
#27182=CARTESIAN_POINT('Ctrl Pts',(-23.1352470274782,20.3542733883821,-31.3506456799688));
#27183=CARTESIAN_POINT('Ctrl Pts',(-23.1094278848446,20.3577880424927,-31.3490543967694));
#27184=CARTESIAN_POINT('Ctrl Pts',(-23.1032964649168,20.3586406885014,-31.3486757982039));
#27185=CARTESIAN_POINT('Ctrl Pts',(-23.0938317763761,20.3599846732642,-31.3480902739741));
#27186=CARTESIAN_POINT('Ctrl Pts',(-23.0904967344325,20.3604635855156,-31.3478837425613));
#27187=CARTESIAN_POINT('Ctrl Pts',(-23.0838530841978,20.3614282498084,-31.3474718914821));
#27188=CARTESIAN_POINT('Ctrl Pts',(-23.0805444686026,20.3619139234685,-31.347266574539));
#27189=CARTESIAN_POINT('Ctrl Pts',(-23.0732061684528,20.3630027874709,-31.3468107253183));
#27190=CARTESIAN_POINT('Ctrl Pts',(-23.0691768647877,20.3636084713698,-31.3465601141707));
#27191=CARTESIAN_POINT('Ctrl Pts',(-23.0575379845299,20.3653806027337,-31.3458352954368));
#27192=CARTESIAN_POINT('Ctrl Pts',(-23.0499314639139,20.3665666715071,-31.345360465199));
#27193=CARTESIAN_POINT('Ctrl Pts',(-22.9982436229178,20.3748160605633,-31.3421261273462));
#27194=CARTESIAN_POINT('Ctrl Pts',(-22.9543107943938,20.3827671347366,-31.3393384952434));
#27195=CARTESIAN_POINT('Ctrl Pts',(-22.9007946020738,20.393605384121,-31.3358932618598));
#27196=CARTESIAN_POINT('Ctrl Pts',(-22.8910395103731,20.3956281474638,-31.3352632347512));
#27197=CARTESIAN_POINT('Ctrl Pts',(-22.7562148393406,20.4242373445125,-31.3265275360768));
#27198=CARTESIAN_POINT('Ctrl Pts',(-22.632840817412,20.4581956537457,-31.3181915046303));
#27199=CARTESIAN_POINT('Ctrl Pts',(-22.210310530093,20.6020134004645,-31.288508791225));
#27200=CARTESIAN_POINT('Ctrl Pts',(-21.9256952333279,20.7487587908881,-31.2662788654909));
#27201=CARTESIAN_POINT('Ctrl Pts',(-21.6542858115567,20.9441669564894,-31.2451184715937));
#27202=CARTESIAN_POINT('Ctrl Pts',(-21.6414141517445,20.9535800661338,-31.2441155302391));
#27203=CARTESIAN_POINT('Ctrl Pts',(-21.6257506293052,20.9652142921887,-31.2428963222445));
#27204=CARTESIAN_POINT('Ctrl Pts',(-21.6228921940158,20.9673447902036,-31.2426738812911));
#27205=CARTESIAN_POINT('Ctrl Pts',(-21.6181804980262,20.9708687689621,-31.2423073157127));
#27206=CARTESIAN_POINT('Ctrl Pts',(-21.6163252057177,20.972259506754,-31.2421629999459));
#27207=CARTESIAN_POINT('Ctrl Pts',(-21.6130126149994,20.97474823216,-31.2419053725884));
#27208=CARTESIAN_POINT('Ctrl Pts',(-21.6115547515364,20.9758454525745,-31.2417920074192));
#27209=CARTESIAN_POINT('Ctrl Pts',(-21.6084271104004,20.9782035481762,-31.2415488331755));
#27210=CARTESIAN_POINT('Ctrl Pts',(-21.6067576331428,20.9794648081037,-31.2414190522702));
#27211=CARTESIAN_POINT('Ctrl Pts',(-21.6033227858814,20.9820650313965,-31.2411520766157));
#27212=CARTESIAN_POINT('Ctrl Pts',(-21.6015575653926,20.9834041917648,-31.2410148958836));
#27213=CARTESIAN_POINT('Ctrl Pts',(-21.5971337313606,20.9867674664976,-31.2406711577194));
#27214=CARTESIAN_POINT('Ctrl Pts',(-21.594476874384,20.9887939030586,-31.2404647630279));
#27215=CARTESIAN_POINT('Ctrl Pts',(-21.5869862659899,20.994525584977,-31.2398829814991));
#27216=CARTESIAN_POINT('Ctrl Pts',(-21.5821598278555,20.998240430091,-31.2395082592389));
#27217=CARTESIAN_POINT('Ctrl Pts',(-21.5375901287719,21.0327467719972,-31.2360488699788));
#27218=CARTESIAN_POINT('Ctrl Pts',(-21.4985593411228,21.0644526761777,-31.2330266140962));
#27219=CARTESIAN_POINT('Ctrl Pts',(-21.4103840409328,21.1395726183558,-31.226173877576));
#27220=CARTESIAN_POINT('Ctrl Pts',(-21.3617898444017,21.1835994364965,-31.2223782813598));
#27221=CARTESIAN_POINT('Ctrl Pts',(-21.1000448549493,21.4357042791965,-31.2016080923626));
#27222=CARTESIAN_POINT('Ctrl Pts',(-20.9152016390504,21.6710633347323,-31.1855464329415));
#27223=CARTESIAN_POINT('Ctrl Pts',(-20.7191388197885,22.0077453333449,-31.162798688452));
#27224=CARTESIAN_POINT('Ctrl Pts',(-20.6763836762828,22.0889487800925,-31.1573411403017));
#27225=CARTESIAN_POINT('Ctrl Pts',(-20.6332280755213,22.1801539651271,-31.1511987777575));
#27226=CARTESIAN_POINT('Ctrl Pts',(-20.6293389435296,22.1884648948877,-31.1506389702535));
#27227=CARTESIAN_POINT('Ctrl Pts',(-20.6236027006337,22.2008606592959,-31.1498038352257));
#27228=CARTESIAN_POINT('Ctrl Pts',(-20.621728510578,22.2049329724979,-31.1495294438701));
#27229=CARTESIAN_POINT('Ctrl Pts',(-20.6185280839479,22.2119253628992,-31.149058243651));
#27230=CARTESIAN_POINT('Ctrl Pts',(-20.6171976944573,22.2148435419469,-31.1488615782981));
#27231=CARTESIAN_POINT('Ctrl Pts',(-20.6146125865771,22.220536415976,-31.148477883503));
#27232=CARTESIAN_POINT('Ctrl Pts',(-20.6133574404032,22.2233109133766,-31.1482908690904));
#27233=CARTESIAN_POINT('Ctrl Pts',(-20.6103562353584,22.2299701870663,-31.147841962428));
#27234=CARTESIAN_POINT('Ctrl Pts',(-20.6086139450114,22.2338566460266,-31.1475799409189));
#27235=CARTESIAN_POINT('Ctrl Pts',(-20.6033817501196,22.2455901558354,-31.1467887737845));
#27236=CARTESIAN_POINT('Ctrl Pts',(-20.5999155239155,22.2534476672209,-31.1462588164598));
#27237=CARTESIAN_POINT('Ctrl Pts',(-20.5682748950425,22.3259565941175,-31.1413669215099));
#27238=CARTESIAN_POINT('Ctrl Pts',(-20.5422002916347,22.3914981919462,-31.1369337551516));
#27239=CARTESIAN_POINT('Ctrl Pts',(-20.4787304662932,22.5676563085786,-31.1249744274318));
#27240=CARTESIAN_POINT('Ctrl Pts',(-20.4451626688475,22.679531529205,-31.1173310898589));
#27241=CARTESIAN_POINT('Ctrl Pts',(-20.3531744804519,23.060042885716,-31.0912524807817));
#27242=CARTESIAN_POINT('Ctrl Pts',(-20.3230315876301,23.3342594172357,-31.0722239809687));
#27243=CARTESIAN_POINT('Ctrl Pts',(-20.3289571149693,23.6594370364511,-31.051135404293));
#27244=CARTESIAN_POINT('Ctrl Pts',(-20.3310623846339,23.7098800000633,-31.0479099357925));
#27245=CARTESIAN_POINT('Ctrl Pts',(-20.3346852960567,23.7653596522754,-31.044428020615));
#27246=CARTESIAN_POINT('Ctrl Pts',(-20.3350307202184,23.7704624862737,-31.0441083786154));
#27247=CARTESIAN_POINT('Ctrl Pts',(-20.335562804414,23.7780545300027,-31.0436337463751));
#27248=CARTESIAN_POINT('Ctrl Pts',(-20.3357402090904,23.7805443488446,-31.0434782397668));
#27249=CARTESIAN_POINT('Ctrl Pts',(-20.3360494333168,23.7848142311195,-31.043211815167));
#27250=CARTESIAN_POINT('Ctrl Pts',(-20.3361798389581,23.7865943906608,-31.0431008172558));
#27251=CARTESIAN_POINT('Ctrl Pts',(-20.3364487973374,23.7902245324426,-31.0428746268244));
#27252=CARTESIAN_POINT('Ctrl Pts',(-20.3365874682379,23.7920744993528,-31.0427594417227));
#27253=CARTESIAN_POINT('Ctrl Pts',(-20.336913973075,23.7963804194966,-31.0424915356239));
#27254=CARTESIAN_POINT('Ctrl Pts',(-20.3371030257961,23.7988362848051,-31.042338883861));
#27255=CARTESIAN_POINT('Ctrl Pts',(-20.3375076276058,23.8040146290227,-31.0420173146262));
#27256=CARTESIAN_POINT('Ctrl Pts',(-20.3377238222434,23.8067370572855,-31.0418484336281));
#27257=CARTESIAN_POINT('Ctrl Pts',(-20.3383114561585,23.8140195150221,-31.0413971495107));
#27258=CARTESIAN_POINT('Ctrl Pts',(-20.3386891473511,23.818579055089,-31.0411150942539));
#27259=CARTESIAN_POINT('Ctrl Pts',(-20.3398712056426,23.8324889194978,-31.0402560870281));
#27260=CARTESIAN_POINT('Ctrl Pts',(-20.3407067156359,23.8418366480163,-31.0396808340372));
#27261=CARTESIAN_POINT('Ctrl Pts',(-20.3439057351248,23.8759464335914,-31.0375886768354));
#27262=CARTESIAN_POINT('Ctrl Pts',(-20.3465151394298,23.9006852692491,-31.0360846485061));
#27263=CARTESIAN_POINT('Ctrl Pts',(-20.3614725686483,24.0283080230706,-31.028383288618));
#27264=CARTESIAN_POINT('Ctrl Pts',(-20.3784920495251,24.1305922333574,-31.0224039191853));
#27265=CARTESIAN_POINT('Ctrl Pts',(-20.4758542060815,24.5805036920593,-30.9962779180317));
#27266=CARTESIAN_POINT('Ctrl Pts',(-20.6086304496797,24.9141463597551,-30.9770522312961));
#27267=CARTESIAN_POINT('Ctrl Pts',(-20.8041219539098,25.2370591183088,-30.9542295987389));
#27268=CARTESIAN_POINT('Ctrl Pts',(-20.8150582393367,25.2547353748124,-30.9529667279983));
#27269=CARTESIAN_POINT('Ctrl Pts',(-20.8295315910889,25.2776305539875,-30.9513127713045));
#27270=CARTESIAN_POINT('Ctrl Pts',(-20.8329142233263,25.2829469033408,-30.9509274235007));
#27271=CARTESIAN_POINT('Ctrl Pts',(-20.8381414640695,25.2911093960815,-30.9503337719367));
#27272=CARTESIAN_POINT('Ctrl Pts',(-20.8399750233767,25.2939626260578,-30.950125880445));
#27273=CARTESIAN_POINT('Ctrl Pts',(-20.8436071932945,25.2995951322218,-30.949714734929));
#27274=CARTESIAN_POINT('Ctrl Pts',(-20.8454055893282,25.3023745423272,-30.9495114890991));
#27275=CARTESIAN_POINT('Ctrl Pts',(-20.8493998811444,25.3085268906114,-30.9490607889974));
#27276=CARTESIAN_POINT('Ctrl Pts',(-20.8515978166765,25.3118984921771,-30.9488132584748));
#27277=CARTESIAN_POINT('Ctrl Pts',(-20.8578906809884,25.3215122417096,-30.9481059077528));
#27278=CARTESIAN_POINT('Ctrl Pts',(-20.8620009715116,25.327744259701,-30.9476455105892));
#27279=CARTESIAN_POINT('Ctrl Pts',(-20.8882461781951,25.3672379558742,-30.9447159278817));
#27280=CARTESIAN_POINT('Ctrl Pts',(-20.9109755451346,25.4000986372219,-30.942224329423));
#27281=CARTESIAN_POINT('Ctrl Pts',(-20.9803170051858,25.4964678571596,-30.9347507268733));
#27282=CARTESIAN_POINT('Ctrl Pts',(-21.0286502156223,25.5586953994385,-30.9297032613071));
#27283=CARTESIAN_POINT('Ctrl Pts',(-21.1117901697997,25.6579988339002,-30.9212725220757));
#27284=CARTESIAN_POINT('Ctrl Pts',(-21.145282527071,25.6961351128577,-30.9179372410419));
#27285=CARTESIAN_POINT('Ctrl Pts',(-21.2054707436818,25.7614891919763,-30.9120515975798));
#27286=CARTESIAN_POINT('Ctrl Pts',(-21.231775711509,25.7890545112767,-30.9095132581886));
#27287=CARTESIAN_POINT('Ctrl Pts',(-21.4649912632757,26.0249251064988,-30.8873144693889));
#27288=CARTESIAN_POINT('Ctrl Pts',(-21.6989790627461,26.2045159984836,-30.866934320563));
#27289=CARTESIAN_POINT('Ctrl Pts',(-21.9679152640053,26.3578459892651,-30.8473466964458));
#27290=CARTESIAN_POINT('Ctrl Pts',(-21.9818381270953,26.3656474475507,-30.8463429150488));
#27291=CARTESIAN_POINT('Ctrl Pts',(-21.9989425455034,26.3750653761334,-30.8451228128778));
#27292=CARTESIAN_POINT('Ctrl Pts',(-22.0020692552626,26.3767802287538,-30.8449003072546));
#27293=CARTESIAN_POINT('Ctrl Pts',(-22.007233933754,26.379601670035,-30.8445336570458));
#27294=CARTESIAN_POINT('Ctrl Pts',(-22.0092702507424,26.3807112489488,-30.8443893211667));
#27295=CARTESIAN_POINT('Ctrl Pts',(-22.0128516768031,26.3826577395739,-30.8441358662157));
#27296=CARTESIAN_POINT('Ctrl Pts',(-22.014396269705,26.383495583888,-30.844026687041));
#27297=CARTESIAN_POINT('Ctrl Pts',(-22.0177623447085,26.3853179059365,-30.8437890415365));
#27298=CARTESIAN_POINT('Ctrl Pts',(-22.0195840863143,26.3863018894825,-30.8436606073366));
#27299=CARTESIAN_POINT('Ctrl Pts',(-22.0244495363387,26.3889238280697,-30.8433180690589));
#27300=CARTESIAN_POINT('Ctrl Pts',(-22.0274949444745,26.3905586490577,-30.8431041662688));
#27301=CARTESIAN_POINT('Ctrl Pts',(-22.0342064433436,26.3941475858544,-30.8426338534958));
#27302=CARTESIAN_POINT('Ctrl Pts',(-22.0378737014702,26.3960995225607,-30.8423775812223));
#27303=CARTESIAN_POINT('Ctrl Pts',(-22.0488140436608,26.4018955147988,-30.8416151501708));
#27304=CARTESIAN_POINT('Ctrl Pts',(-22.0560981499387,26.4057188549625,-30.841110272455));
#27305=CARTESIAN_POINT('Ctrl Pts',(-22.0672725156933,26.4115296795246,-30.8403398323904));
#27306=CARTESIAN_POINT('Ctrl Pts',(-22.0711522263205,26.413537171993,-30.8400730875419));
#27307=CARTESIAN_POINT('Ctrl Pts',(-22.0750360153473,26.4155367745569,-30.8398067994259));
#27308=CARTESIAN_POINT('Origin',(-23.5502525316942,23.5502525316942,-77.3107734492734));
#27309=CARTESIAN_POINT('',(-22.0750360135777,26.4155367736458,-29.3439103255379));
#27310=CARTESIAN_POINT('',(-22.0750360153461,26.4155367745563,-29.5927618641105));
#27311=CARTESIAN_POINT('',(-22.0750360153461,26.4155367745563,-77.3107734492734));
#27312=CARTESIAN_POINT('Ctrl Pts',(-22.0750360135777,26.4155367736458,-29.3439103255379));
#27313=CARTESIAN_POINT('Ctrl Pts',(-22.0178680196052,26.3861033346239,-29.3476546934872));
#27314=CARTESIAN_POINT('Ctrl Pts',(-21.9615946141282,26.3549660488702,-29.3514478427651));
#27315=CARTESIAN_POINT('Ctrl Pts',(-21.8847349755201,26.3093822712396,-29.3568014974043));
#27316=CARTESIAN_POINT('Ctrl Pts',(-21.8633295656043,26.2963473047052,-29.3583116634764));
#27317=CARTESIAN_POINT('Ctrl Pts',(-21.8326932487767,26.2771977414827,-29.3605019039041));
#27318=CARTESIAN_POINT('Ctrl Pts',(-21.8233380687557,26.2712829432223,-29.3611746482961));
#27319=CARTESIAN_POINT('Ctrl Pts',(-21.8067732576553,26.2606900322315,-29.3623729386914));
#27320=CARTESIAN_POINT('Ctrl Pts',(-21.7995514877892,26.2560310288995,-29.3628977725897));
#27321=CARTESIAN_POINT('Ctrl Pts',(-21.7887921416467,26.2490287101577,-29.3636833449846));
#27322=CARTESIAN_POINT('Ctrl Pts',(-21.7852403766333,26.246707177959,-29.3639432671455));
#27323=CARTESIAN_POINT('Ctrl Pts',(-21.7789872810581,26.2426023328506,-29.3644019340346));
#27324=CARTESIAN_POINT('Ctrl Pts',(-21.7762840274648,26.2408219483375,-29.364600568507));
#27325=CARTESIAN_POINT('Ctrl Pts',(-21.7708981957186,26.237263151053,-29.3649970187144));
#27326=CARTESIAN_POINT('Ctrl Pts',(-21.7682155900993,26.2354847861122,-29.3651948325027));
#27327=CARTESIAN_POINT('Ctrl Pts',(-21.761767325518,26.231196155021,-29.3656711635234));
#27328=CARTESIAN_POINT('Ctrl Pts',(-21.7580042887569,26.2286819743959,-29.3659498284372));
#27329=CARTESIAN_POINT('Ctrl Pts',(-21.7464831292812,26.2209492436591,-29.3668051362848));
#27330=CARTESIAN_POINT('Ctrl Pts',(-21.7387424626994,26.2157048856773,-29.3673827563272));
#27331=CARTESIAN_POINT('Ctrl Pts',(-21.7101508074189,26.1961517571963,-29.3695274202732));
#27332=CARTESIAN_POINT('Ctrl Pts',(-21.6894460663366,26.1816316960969,-29.3711025028214));
#27333=CARTESIAN_POINT('Ctrl Pts',(-21.6640209969043,26.1633511693042,-29.3730646011676));
#27334=CARTESIAN_POINT('Ctrl Pts',(-21.6591370896011,26.1598188321732,-29.3734427924499));
#27335=CARTESIAN_POINT('Ctrl Pts',(-21.648714880122,26.1522362363972,-29.3742526237282));
#27336=CARTESIAN_POINT('Ctrl Pts',(-21.6431795531629,26.1481819559223,-29.37468441725));
#27337=CARTESIAN_POINT('Ctrl Pts',(-21.6363407950832,26.1431393595879,-29.3752199848165));
#27338=CARTESIAN_POINT('Ctrl Pts',(-21.6350250815671,26.1421676638052,-29.375323119516));
#27339=CARTESIAN_POINT('Ctrl Pts',(-21.6314837665997,26.1395481226425,-29.3756009723261));
#27340=CARTESIAN_POINT('Ctrl Pts',(-21.6292595520746,26.1378984122934,-29.3757757620028));
#27341=CARTESIAN_POINT('Ctrl Pts',(-21.6215065602348,26.1321324767796,-29.3763859985233));
#27342=CARTESIAN_POINT('Ctrl Pts',(-21.6159888937043,26.128001404417,-29.3768220143343));
#27343=CARTESIAN_POINT('Ctrl Pts',(-21.6075922613752,26.1216727140609,-29.3774881687768));
#27344=CARTESIAN_POINT('Ctrl Pts',(-21.6047036525534,26.1194878729702,-29.377717817731));
#27345=CARTESIAN_POINT('Ctrl Pts',(-21.5985003974116,26.1147794908042,-29.3782120175689));
#27346=CARTESIAN_POINT('Ctrl Pts',(-21.5951869518569,26.1122543849245,-29.3784766279318));
#27347=CARTESIAN_POINT('Ctrl Pts',(-21.5802653414545,26.1008371416732,-29.379671133859));
#27348=CARTESIAN_POINT('Ctrl Pts',(-21.5687130228502,26.0918725949951,-29.3806037805596));
#27349=CARTESIAN_POINT('Ctrl Pts',(-21.5237318913766,26.0564743641618,-29.384266207618));
#27350=CARTESIAN_POINT('Ctrl Pts',(-21.4907688772662,26.0294581693593,-29.3870177915576));
#27351=CARTESIAN_POINT('Ctrl Pts',(-21.2445470582561,25.8193573905688,-29.4080911069868));
#27352=CARTESIAN_POINT('Ctrl Pts',(-21.0555397480742,25.6097386112236,-29.4274458762233));
#27353=CARTESIAN_POINT('Ctrl Pts',(-20.8373662174436,25.2929815670697,-29.4530975145878));
#27354=CARTESIAN_POINT('Ctrl Pts',(-20.7827271599645,25.2048415278285,-29.4598936185849));
#27355=CARTESIAN_POINT('Ctrl Pts',(-20.7256455166144,25.1019960620047,-29.4673212103159));
#27356=CARTESIAN_POINT('Ctrl Pts',(-20.7189445487789,25.0897355281373,-29.4681988265762));
#27357=CARTESIAN_POINT('Ctrl Pts',(-20.7106204621924,25.0742670284856,-29.4692958628696));
#27358=CARTESIAN_POINT('Ctrl Pts',(-20.7089228237139,25.0710996533412,-29.4695199599921));
#27359=CARTESIAN_POINT('Ctrl Pts',(-20.7062338593202,25.0660624908859,-29.4698754899475));
#27360=CARTESIAN_POINT('Ctrl Pts',(-20.7052390775139,25.0641945671737,-29.4700071435581));
#27361=CARTESIAN_POINT('Ctrl Pts',(-20.7033683078661,25.0606734263678,-29.4702549637882));
#27362=CARTESIAN_POINT('Ctrl Pts',(-20.702491926048,25.0590204382652,-29.4703711550892));
#27363=CARTESIAN_POINT('Ctrl Pts',(-20.7005081999307,25.0552709460492,-29.4706343809338));
#27364=CARTESIAN_POINT('Ctrl Pts',(-20.699401731423,25.0531739862772,-29.4707813589195));
#27365=CARTESIAN_POINT('Ctrl Pts',(-20.696141954228,25.0469795609016,-29.4712148445495));
#27366=CARTESIAN_POINT('Ctrl Pts',(-20.6939951463143,25.0428786528182,-29.4715009385304));
#27367=CARTESIAN_POINT('Ctrl Pts',(-20.6797915815371,25.0156036493566,-29.4733979461197));
#27368=CARTESIAN_POINT('Ctrl Pts',(-20.6680076885269,24.9922874595808,-29.4749918691834));
#27369=CARTESIAN_POINT('Ctrl Pts',(-20.6536477416588,24.9629947168081,-29.4769631282619));
#27370=CARTESIAN_POINT('Ctrl Pts',(-20.6508049473055,24.9571510703622,-29.477354839241));
#27371=CARTESIAN_POINT('Ctrl Pts',(-20.6440280852471,24.9431127748106,-29.4782922640567));
#27372=CARTESIAN_POINT('Ctrl Pts',(-20.6401109531268,24.9349099573782,-29.4788370940603));
#27373=CARTESIAN_POINT('Ctrl Pts',(-20.5485036108483,24.7409702492367,-29.491652241233));
#27374=CARTESIAN_POINT('Ctrl Pts',(-20.4787227531851,24.5472639593954,-29.5030407899759));
#27375=CARTESIAN_POINT('Ctrl Pts',(-20.3847622922454,24.1795985552876,-29.524248206233));
#27376=CARTESIAN_POINT('Ctrl Pts',(-20.3554027693371,24.0077815706142,-29.5340068344254));
#27377=CARTESIAN_POINT('Ctrl Pts',(-20.3345864680789,23.7726456518554,-29.5477977963679));
#27378=CARTESIAN_POINT('Ctrl Pts',(-20.3309013420733,23.7107022381336,-29.5514690400063));
#27379=CARTESIAN_POINT('Ctrl Pts',(-20.3283426521953,23.626975527394,-29.5565006900676));
#27380=CARTESIAN_POINT('Ctrl Pts',(-20.3278986134397,23.6052514403914,-29.5578124777193));
#27381=CARTESIAN_POINT('Ctrl Pts',(-20.3275715248233,23.5735714598629,-29.5597351966069));
#27382=CARTESIAN_POINT('Ctrl Pts',(-20.3275148733939,23.5636176640317,-29.5603407145013));
#27383=CARTESIAN_POINT('Ctrl Pts',(-20.3274959959025,23.5457836877933,-29.5614281862632));
#27384=CARTESIAN_POINT('Ctrl Pts',(-20.3275165572314,23.5379035755246,-29.5619095984465));
#27385=CARTESIAN_POINT('Ctrl Pts',(-20.3275917209395,23.5259291449268,-29.562642538152));
#27386=CARTESIAN_POINT('Ctrl Pts',(-20.3276252255884,23.5218346849459,-29.5628934030969));
#27387=CARTESIAN_POINT('Ctrl Pts',(-20.3276971372912,23.5147068521127,-29.5633305569627));
#27388=CARTESIAN_POINT('Ctrl Pts',(-20.3277320245295,23.5116734423643,-29.5635167351411));
#27389=CARTESIAN_POINT('Ctrl Pts',(-20.3278130012697,23.5054025759249,-29.5639019011689));
#27390=CARTESIAN_POINT('Ctrl Pts',(-20.327859686684,23.5021651313347,-29.5641009075339));
#27391=CARTESIAN_POINT('Ctrl Pts',(-20.3279844528735,23.4943318896531,-29.5645828024794));
#27392=CARTESIAN_POINT('Ctrl Pts',(-20.328067487074,23.4897361877984,-29.5648658463594));
#27393=CARTESIAN_POINT('Ctrl Pts',(-20.3284119160133,23.472691946768,-29.5659167782128));
#27394=CARTESIAN_POINT('Ctrl Pts',(-20.328735619331,23.4602449011797,-29.5666866204059));
#27395=CARTESIAN_POINT('Ctrl Pts',(-20.3355574378041,23.2457656474243,-29.5799937603329));
#27396=CARTESIAN_POINT('Ctrl Pts',(-20.3609750653052,23.0448238380425,-29.5931434484847));
#27397=CARTESIAN_POINT('Ctrl Pts',(-20.4695336815122,22.5588805452749,-29.6264839085009));
#27398=CARTESIAN_POINT('Ctrl Pts',(-20.5734868528602,22.2804003586288,-29.6470235236238));
#27399=CARTESIAN_POINT('Ctrl Pts',(-20.7198542289663,22.0091112912566,-29.6664610660877));
#27400=CARTESIAN_POINT('Ctrl Pts',(-20.7257963594688,21.9982479511263,-29.6672381357626));
#27401=CARTESIAN_POINT('Ctrl Pts',(-20.7334716707122,21.984406111499,-29.6682263614525));
#27402=CARTESIAN_POINT('Ctrl Pts',(-20.7351471143684,21.9813959671733,-29.668441152554));
#27403=CARTESIAN_POINT('Ctrl Pts',(-20.7378433631286,21.976570044646,-29.6687853172609));
#27404=CARTESIAN_POINT('Ctrl Pts',(-20.7388611017096,21.974752570113,-29.6689148880571));
#27405=CARTESIAN_POINT('Ctrl Pts',(-20.7407994797359,21.9712988794009,-29.6691610219957));
#27406=CARTESIAN_POINT('Ctrl Pts',(-20.7417197800179,21.9696624931244,-29.6692776054535));
#27407=CARTESIAN_POINT('Ctrl Pts',(-20.7438336168351,21.9659115543129,-29.6695447561175));
#27408=CARTESIAN_POINT('Ctrl Pts',(-20.7450281120055,21.9637975485434,-29.669695260203));
#27409=CARTESIAN_POINT('Ctrl Pts',(-20.7487242609105,21.9572733672647,-29.6701595612308));
#27410=CARTESIAN_POINT('Ctrl Pts',(-20.7512339494578,21.9528677166186,-29.6704728399794));
#27411=CARTESIAN_POINT('Ctrl Pts',(-20.770526498855,21.9191855432891,-29.6728661176289));
#27412=CARTESIAN_POINT('Ctrl Pts',(-20.7877586611584,21.8901669393629,-29.6749175545129));
#27413=CARTESIAN_POINT('Ctrl Pts',(-20.8093909820106,21.8550085227891,-29.6773968778175));
#27414=CARTESIAN_POINT('Ctrl Pts',(-20.8133601924533,21.8486078537924,-29.6778479909058));
#27415=CARTESIAN_POINT('Ctrl Pts',(-20.8181976230589,21.8408678220982,-29.6783932675793));
#27416=CARTESIAN_POINT('Ctrl Pts',(-20.819044410989,21.8395151729472,-29.678488551549));
#27417=CARTESIAN_POINT('Ctrl Pts',(-20.8233726044137,21.8326127718551,-29.6789747325476));
#27418=CARTESIAN_POINT('Ctrl Pts',(-20.8268699477001,21.8270729749063,-29.679364800089));
#27419=CARTESIAN_POINT('Ctrl Pts',(-20.8318244887076,21.8192777348539,-29.6799135416402));
#27420=CARTESIAN_POINT('Ctrl Pts',(-20.8332676266793,21.8170134257934,-29.6800729201709));
#27421=CARTESIAN_POINT('Ctrl Pts',(-20.8403392056938,21.8059485279323,-29.6808516821647));
#27422=CARTESIAN_POINT('Ctrl Pts',(-20.846007644706,21.797173443852,-29.6814690798452));
#27423=CARTESIAN_POINT('Ctrl Pts',(-20.9285584498409,21.6707329957657,-29.6903645643389));
#27424=CARTESIAN_POINT('Ctrl Pts',(-21.013022656774,21.5581819596051,-29.6982795084682));
#27425=CARTESIAN_POINT('Ctrl Pts',(-21.2408970703335,21.2926398740057,-29.7178652504914));
#27426=CARTESIAN_POINT('Ctrl Pts',(-21.3923631804421,21.1474532628132,-29.7294602028303));
#27427=CARTESIAN_POINT('Ctrl Pts',(-21.6272380310684,20.9625583051563,-29.7468655659453));
#27428=CARTESIAN_POINT('Ctrl Pts',(-21.6999182033129,20.9100997314028,-29.7521774371936));
#27429=CARTESIAN_POINT('Ctrl Pts',(-21.7839123618448,20.8546482895322,-29.7582790555064));
#27430=CARTESIAN_POINT('Ctrl Pts',(-21.7931713010991,20.8486038923756,-29.7589511416509));
#27431=CARTESIAN_POINT('Ctrl Pts',(-21.809680239358,20.8379473332529,-29.760148670272));
#27432=CARTESIAN_POINT('Ctrl Pts',(-21.816917956813,20.8333162711962,-29.7606734037356));
#27433=CARTESIAN_POINT('Ctrl Pts',(-21.8277546186596,20.8264433461016,-29.7614586800626));
#27434=CARTESIAN_POINT('Ctrl Pts',(-21.8313396483493,20.8241795247618,-29.7617184066143));
#27435=CARTESIAN_POINT('Ctrl Pts',(-21.8376702830193,20.8201994025288,-29.7621769409948));
#27436=CARTESIAN_POINT('Ctrl Pts',(-21.8404140321721,20.8184801487952,-29.7623756390624));
#27437=CARTESIAN_POINT('Ctrl Pts',(-21.8458915249443,20.8150593959817,-29.7627722440192));
#27438=CARTESIAN_POINT('Ctrl Pts',(-21.8486252371749,20.8133578531583,-29.7629701490033));
#27439=CARTESIAN_POINT('Ctrl Pts',(-21.8552118826738,20.8092718145734,-29.7634469072589));
#27440=CARTESIAN_POINT('Ctrl Pts',(-21.8590672961273,20.806891346554,-29.7637259087937));
#27441=CARTESIAN_POINT('Ctrl Pts',(-21.8709126337061,20.7996120777616,-29.7645829255367));
#27442=CARTESIAN_POINT('Ctrl Pts',(-21.8789188640216,20.7947400261683,-29.7651619231961));
#27443=CARTESIAN_POINT('Ctrl Pts',(-21.9724172570428,20.7384006129698,-29.7719208478736));
#27444=CARTESIAN_POINT('Ctrl Pts',(-22.0602255887921,20.6909009412967,-29.7782445824907));
#27445=CARTESIAN_POINT('Ctrl Pts',(-22.3819606330559,20.5357067558023,-29.8013675934019));
#27446=CARTESIAN_POINT('Ctrl Pts',(-22.6263770501641,20.4520579569957,-29.8189404587776));
#27447=CARTESIAN_POINT('Ctrl Pts',(-22.9533205482786,20.382334018617,-29.8414493446333));
#27448=CARTESIAN_POINT('Ctrl Pts',(-23.0291113477924,20.3689872783488,-29.8465917825679));
#27449=CARTESIAN_POINT('Ctrl Pts',(-23.1572388236527,20.3511266032592,-29.8550899336988));
#27450=CARTESIAN_POINT('Ctrl Pts',(-23.2093391404665,20.345155772925,-29.8584916769161));
#27451=CARTESIAN_POINT('Ctrl Pts',(-23.2866758290401,20.3382001449357,-29.8634397232182));
#27452=CARTESIAN_POINT('Ctrl Pts',(-23.3118131919861,20.3362363539057,-29.8650322106239));
#27453=CARTESIAN_POINT('Ctrl Pts',(-23.3412706070281,20.334282588203,-29.8668778505859));
#27454=CARTESIAN_POINT('Ctrl Pts',(-23.3455698655681,20.334006096954,-29.8671467070072));
#27455=CARTESIAN_POINT('Ctrl Pts',(-23.3521377209585,20.3335969318248,-29.8675566367083));
#27456=CARTESIAN_POINT('Ctrl Pts',(-23.3544059038064,20.3334580364201,-29.8676980595864));
#27457=CARTESIAN_POINT('Ctrl Pts',(-23.3585172869121,20.3332106346201,-29.8679541427334));
#27458=CARTESIAN_POINT('Ctrl Pts',(-23.3603604268506,20.3331013135838,-29.8680688486836));
#27459=CARTESIAN_POINT('Ctrl Pts',(-23.3643819693845,20.3328662543343,-29.8683189145969));
#27460=CARTESIAN_POINT('Ctrl Pts',(-23.3665604002292,20.3327411448328,-29.8684542383228));
#27461=CARTESIAN_POINT('Ctrl Pts',(-23.3725198130563,20.3324049617285,-29.8688240719535));
#27462=CARTESIAN_POINT('Ctrl Pts',(-23.3763010579012,20.3321983388747,-29.8690583304702));
#27463=CARTESIAN_POINT('Ctrl Pts',(-23.3946494961498,20.331228138621,-29.8701931602841));
#27464=CARTESIAN_POINT('Ctrl Pts',(-23.4092216979807,20.3305567897318,-29.8710886048444));
#27465=CARTESIAN_POINT('Ctrl Pts',(-23.4325845243015,20.3296393727334,-29.8725155990318));
#27466=CARTESIAN_POINT('Ctrl Pts',(-23.4413722550516,20.3293303083371,-29.8730503965846));
#27467=CARTESIAN_POINT('Ctrl Pts',(-23.4552246608118,20.3288998764988,-29.8738904909778));
#27468=CARTESIAN_POINT('Ctrl Pts',(-23.4602884691847,20.32875448055,-29.8741969752191));
#27469=CARTESIAN_POINT('Ctrl Pts',(-23.4692961088083,20.3285171015429,-29.8747410953382));
#27470=CARTESIAN_POINT('Ctrl Pts',(-23.4732397926475,20.3284204189589,-29.8749789573932));
#27471=CARTESIAN_POINT('Ctrl Pts',(-23.5803222991823,20.3259919310898,-29.8814280122492));
#27472=CARTESIAN_POINT('Ctrl Pts',(-23.6835242716581,20.3286064585765,-29.8874025397333));
#27473=CARTESIAN_POINT('Ctrl Pts',(-24.0285862726569,20.353962550305,-29.9070860077399));
#27474=CARTESIAN_POINT('Ctrl Pts',(-24.2679519370511,20.3990644558192,-29.9203144092884));
#27475=CARTESIAN_POINT('Ctrl Pts',(-24.5505743434249,20.4862231225292,-29.9372986458494));
#27476=CARTESIAN_POINT('Ctrl Pts',(-24.6007670061799,20.5030671259447,-29.9403667958796));
#27477=CARTESIAN_POINT('Ctrl Pts',(-24.7210768166272,20.5467673770786,-29.9478724683544));
#27478=CARTESIAN_POINT('Ctrl Pts',(-24.7907115036365,20.5748512547966,-29.9523441954129));
#27479=CARTESIAN_POINT('Ctrl Pts',(-24.868407917047,20.6093881481318,-29.9575042744246));
#27480=CARTESIAN_POINT('Ctrl Pts',(-24.8774985147824,20.6134796362641,-29.9581106953332));
#27481=CARTESIAN_POINT('Ctrl Pts',(-24.8937548436343,20.6208871665473,-29.9592000183315));
#27482=CARTESIAN_POINT('Ctrl Pts',(-24.9009276764422,20.6241875022867,-29.9596823779508));
#27483=CARTESIAN_POINT('Ctrl Pts',(-24.9118019608451,20.6292394398509,-29.9604162867224));
#27484=CARTESIAN_POINT('Ctrl Pts',(-24.9155123577214,20.6309718089936,-29.9606671697497));
#27485=CARTESIAN_POINT('Ctrl Pts',(-24.921965761614,20.6339998711249,-29.9611043425421));
#27486=CARTESIAN_POINT('Ctrl Pts',(-24.9247102655843,20.6352923770674,-29.9612905215306));
#27487=CARTESIAN_POINT('Ctrl Pts',(-24.9303801549335,20.6379723616087,-29.9616756857563));
#27488=CARTESIAN_POINT('Ctrl Pts',(-24.9333052816768,20.6393603770194,-29.9618746895022));
#27489=CARTESIAN_POINT('Ctrl Pts',(-24.9412253582447,20.643133202324,-29.9624143161514));
#27490=CARTESIAN_POINT('Ctrl Pts',(-24.9462162471045,20.6455264681822,-29.9627552331826));
#27491=CARTESIAN_POINT('Ctrl Pts',(-24.9647861974285,20.6544901738789,-29.9640269622098));
#27492=CARTESIAN_POINT('Ctrl Pts',(-24.9783250739995,20.6611429931159,-29.9649606468073));
#27493=CARTESIAN_POINT('Ctrl Pts',(-25.0089915469142,20.676480304755,-29.9670905329614));
#27494=CARTESIAN_POINT('Ctrl Pts',(-25.0260891053785,20.6852232632828,-29.9682887668945));
#27495=CARTESIAN_POINT('Ctrl Pts',(-25.0464773044485,20.6958798418967,-29.969730731327));
#27496=CARTESIAN_POINT('Ctrl Pts',(-25.0498442633546,20.6976472906906,-29.9699692921683));
#27497=CARTESIAN_POINT('Ctrl Pts',(-25.0572871008995,20.7015711467992,-29.970497600275));
#27498=CARTESIAN_POINT('Ctrl Pts',(-25.0613614899503,20.7037303481606,-29.9707874454732));
#27499=CARTESIAN_POINT('Ctrl Pts',(-25.0711318546157,20.7089349910903,-29.9714840264801));
#27500=CARTESIAN_POINT('Ctrl Pts',(-25.0768233194982,20.7119888176816,-29.9718910560287));
#27501=CARTESIAN_POINT('Ctrl Pts',(-25.0841663774437,20.7159573035311,-29.9724178296406));
#27502=CARTESIAN_POINT('Ctrl Pts',(-25.085826430652,20.7168563491271,-29.9725370258026));
#27503=CARTESIAN_POINT('Ctrl Pts',(-25.0935890551594,20.7210692289107,-29.9730949078344));
#27504=CARTESIAN_POINT('Ctrl Pts',(-25.0996816595853,20.7244013038612,-29.9735342314657));
#27505=CARTESIAN_POINT('Ctrl Pts',(-25.1100426696915,20.7301113717904,-29.974283841551));
#27506=CARTESIAN_POINT('Ctrl Pts',(-25.1143165425432,20.7324794382877,-29.9745937808011));
#27507=CARTESIAN_POINT('Ctrl Pts',(-25.1220899392833,20.7368096544886,-29.9751588337431));
#27508=CARTESIAN_POINT('Ctrl Pts',(-25.1255912220107,20.7387686406224,-29.9754138371047));
#27509=CARTESIAN_POINT('Ctrl Pts',(-25.133468711454,20.7431954727536,-29.9759886783919));
#27510=CARTESIAN_POINT('Ctrl Pts',(-25.137842816619,20.7456670202929,-29.9763086439246));
#27511=CARTESIAN_POINT('Ctrl Pts',(-25.1573788527386,20.7567660240735,-29.9777411800791));
#27512=CARTESIAN_POINT('Ctrl Pts',(-25.172476144904,20.7655061500406,-29.9788576187743));
#27513=CARTESIAN_POINT('Ctrl Pts',(-25.2071090662918,20.7859330518737,-29.981440477589));
#27514=CARTESIAN_POINT('Ctrl Pts',(-25.2265931529087,20.7977050126855,-29.9829097270072));
#27515=CARTESIAN_POINT('Ctrl Pts',(-25.3325497949153,20.8632645283129,-29.9909884532556));
#27516=CARTESIAN_POINT('Ctrl Pts',(-25.4165538316109,20.9209171537859,-29.9977228300741));
#27517=CARTESIAN_POINT('Ctrl Pts',(-25.555793132434,21.0265164871294,-30.0094254298211));
#27518=CARTESIAN_POINT('Ctrl Pts',(-25.6123897533205,21.0725466813383,-30.0143486467559));
#27519=CARTESIAN_POINT('Ctrl Pts',(-25.7843945942848,21.2224173576041,-30.0297844763344));
#27520=CARTESIAN_POINT('Ctrl Pts',(-25.8939017044282,21.3327041494442,-30.0403263721104));
#27521=CARTESIAN_POINT('Ctrl Pts',(-26.0396786864498,21.5024319866593,-30.0550241421539));
#27522=CARTESIAN_POINT('Ctrl Pts',(-26.0826536977781,21.5558209040924,-30.0594523360189));
#27523=CARTESIAN_POINT('Ctrl Pts',(-26.1305212028653,21.619332474965,-30.0644608289943));
#27524=CARTESIAN_POINT('Ctrl Pts',(-26.1371001740058,21.6281552488437,-30.0651509600491));
#27525=CARTESIAN_POINT('Ctrl Pts',(-26.1455936015387,21.6396680164257,-30.0660440282673));
#27526=CARTESIAN_POINT('Ctrl Pts',(-26.1475491984386,21.6423273539272,-30.0662498027954));
#27527=CARTESIAN_POINT('Ctrl Pts',(-26.1507131027957,21.6466436994435,-30.0665829521676));
#27528=CARTESIAN_POINT('Ctrl Pts',(-26.1519239142178,21.648298855736,-30.0667105023748));
#27529=CARTESIAN_POINT('Ctrl Pts',(-26.1542454935481,21.6514787758734,-30.0669551688019));
#27530=CARTESIAN_POINT('Ctrl Pts',(-26.1553564992659,21.6530033547712,-30.0670723014382));
#27531=CARTESIAN_POINT('Ctrl Pts',(-26.157908217494,21.6565114203862,-30.0673414352144));
#27532=CARTESIAN_POINT('Ctrl Pts',(-26.1593480094013,21.6584955809613,-30.0674933716782));
#27533=CARTESIAN_POINT('Ctrl Pts',(-26.163798106624,21.6646429526951,-30.0679632281952));
#27534=CARTESIAN_POINT('Ctrl Pts',(-26.1668007407994,21.6688117468322,-30.0682806154101));
#27535=CARTESIAN_POINT('Ctrl Pts',(-26.1912655746108,21.7029500488124,-30.0708697227064));
#27536=CARTESIAN_POINT('Ctrl Pts',(-26.2122232150547,21.7332801264855,-30.0731072706912));
#27537=CARTESIAN_POINT('Ctrl Pts',(-26.401834456812,22.0180125257273,-30.0936045308531));
#27538=CARTESIAN_POINT('Ctrl Pts',(-26.5340888704572,22.2948407039127,-30.1099427983761));
#27539=CARTESIAN_POINT('Ctrl Pts',(-26.656866147206,22.68647214118,-30.1332533022025));
#27540=CARTESIAN_POINT('Ctrl Pts',(-26.683380540385,22.7882349637176,-30.1393122610416));
#27541=CARTESIAN_POINT('Ctrl Pts',(-26.7184296737575,22.9559771439133,-30.1494398378854));
#27542=CARTESIAN_POINT('Ctrl Pts',(-26.7299793276157,23.0212476397247,-30.1534137343236));
#27543=CARTESIAN_POINT('Ctrl Pts',(-26.7407269052554,23.095211152118,-30.1579693586841));
#27544=CARTESIAN_POINT('Ctrl Pts',(-26.7419124831522,23.1036026267634,-30.158486962878));
#27545=CARTESIAN_POINT('Ctrl Pts',(-26.7436409838326,23.116195277371,-30.1592648597348));
#27546=CARTESIAN_POINT('Ctrl Pts',(-26.7442087515706,23.1203930528824,-30.1595243648907));
#27547=CARTESIAN_POINT('Ctrl Pts',(-26.745169978138,23.1276069065558,-30.1599706576229));
#27548=CARTESIAN_POINT('Ctrl Pts',(-26.7455674473661,23.1306224521967,-30.160157317942));
#27549=CARTESIAN_POINT('Ctrl Pts',(-26.7463762991624,23.1368268868681,-30.1605415767201));
#27550=CARTESIAN_POINT('Ctrl Pts',(-26.7467871795949,23.1400158373105,-30.1607391908765));
#27551=CARTESIAN_POINT('Ctrl Pts',(-26.7477633900233,23.1476829759905,-30.1612145855562));
#27552=CARTESIAN_POINT('Ctrl Pts',(-26.7483240844621,23.152161738826,-30.1614925124879));
#27553=CARTESIAN_POINT('Ctrl Pts',(-26.7500113936267,23.1658734166126,-30.1623440788993));
#27554=CARTESIAN_POINT('Ctrl Pts',(-26.751107439879,23.175109982171,-30.1629186838432));
#27555=CARTESIAN_POINT('Ctrl Pts',(-26.7631557277501,23.2805415000219,-30.1694888280347));
#27556=CARTESIAN_POINT('Ctrl Pts',(-26.7698068178985,23.3771689334649,-30.1756196284918));
#27557=CARTESIAN_POINT('Ctrl Pts',(-26.7727190415123,23.5001227090048,-30.1835710666304));
#27558=CARTESIAN_POINT('Ctrl Pts',(-26.773019992036,23.5263099891905,-30.1852730874953));
#27559=CARTESIAN_POINT('Ctrl Pts',(-26.7727881413319,23.8591445991835,-30.2070111173044));
#27560=CARTESIAN_POINT('Ctrl Pts',(-26.7288145915301,24.1641331308318,-30.2282816487434));
#27561=CARTESIAN_POINT('Ctrl Pts',(-26.6200796999562,24.5344139073553,-30.2536889018559));
#27562=CARTESIAN_POINT('Ctrl Pts',(-26.5949190042235,24.609696273329,-30.2588187780465));
#27563=CARTESIAN_POINT('Ctrl Pts',(-26.5648100570725,24.6898135548397,-30.2641831682948));
#27564=CARTESIAN_POINT('Ctrl Pts',(-26.5626008004105,24.69564081031,-30.2645727891766));
#27565=CARTESIAN_POINT('Ctrl Pts',(-26.5595004538812,24.7037474359697,-30.2651140049904));
#27566=CARTESIAN_POINT('Ctrl Pts',(-26.5586236682179,24.7060322063748,-30.2652664516389));
#27567=CARTESIAN_POINT('Ctrl Pts',(-26.5571075767115,24.7099694972708,-30.265529002119));
#27568=CARTESIAN_POINT('Ctrl Pts',(-26.5564695106695,24.7116224888342,-30.2656391807735));
#27569=CARTESIAN_POINT('Ctrl Pts',(-26.5551441303917,24.7150476448031,-30.2658673810035));
#27570=CARTESIAN_POINT('Ctrl Pts',(-26.5544566126293,24.7168197245953,-30.2659853894375));
#27571=CARTESIAN_POINT('Ctrl Pts',(-26.5528310619855,24.7209986205535,-30.266263545387));
#27572=CARTESIAN_POINT('Ctrl Pts',(-26.551891699791,24.7234049258035,-30.2664236122652));
#27573=CARTESIAN_POINT('Ctrl Pts',(-26.5487986489507,24.7313001648601,-30.2669484756866));
#27574=CARTESIAN_POINT('Ctrl Pts',(-26.5466327734298,24.7367843590633,-30.2673125387166));
#27575=CARTESIAN_POINT('Ctrl Pts',(-26.5000259625355,24.8538555828179,-30.2750737539433));
#27576=CARTESIAN_POINT('Ctrl Pts',(-26.4493901276216,24.9628929750652,-30.282100310551));
#27577=CARTESIAN_POINT('Ctrl Pts',(-26.2525711616475,25.3312978359722,-30.3059732692979));
#27578=CARTESIAN_POINT('Ctrl Pts',(-26.0767028823639,25.5730501660351,-30.3220187358018));
#27579=CARTESIAN_POINT('Ctrl Pts',(-25.8062139033024,25.8535635513256,-30.3447669706851));
#27580=CARTESIAN_POINT('Ctrl Pts',(-25.7394636572377,25.9170975895764,-30.3502465928779));
#27581=CARTESIAN_POINT('Ctrl Pts',(-25.6624018828405,25.9843944398709,-30.3564747648856));
#27582=CARTESIAN_POINT('Ctrl Pts',(-25.6546833073551,25.9910705948392,-30.3570975201256));
#27583=CARTESIAN_POINT('Ctrl Pts',(-25.6438091903555,26.0003862018332,-30.3579734393602));
#27584=CARTESIAN_POINT('Ctrl Pts',(-25.6406800497583,26.0030564937015,-30.3582253288853));
#27585=CARTESIAN_POINT('Ctrl Pts',(-25.6349368787238,26.0079385288728,-30.3586873443334));
#27586=CARTESIAN_POINT('Ctrl Pts',(-25.6323244157136,26.0101521144245,-30.35889739407));
#27587=CARTESIAN_POINT('Ctrl Pts',(-25.6270299040134,26.0146237700862,-30.3593228634635));
#27588=CARTESIAN_POINT('Ctrl Pts',(-25.6243476892283,26.0168816347677,-30.3595382910953));
#27589=CARTESIAN_POINT('Ctrl Pts',(-25.6177480198142,26.022418802283,-30.3600680749249));
#27590=CARTESIAN_POINT('Ctrl Pts',(-25.613826451375,26.0256931672915,-30.3603826324934));
#27591=CARTESIAN_POINT('Ctrl Pts',(-25.5995684669787,26.0375406331669,-30.3615254288376));
#27592=CARTESIAN_POINT('Ctrl Pts',(-25.5891863872528,26.0460583386876,-30.3623559179686));
#27593=CARTESIAN_POINT('Ctrl Pts',(-25.437248566063,26.1691309932815,-30.3744868818276));
#27594=CARTESIAN_POINT('Ctrl Pts',(-25.286311467082,26.2715311269103,-30.3862789528047));
#27595=CARTESIAN_POINT('Ctrl Pts',(-24.8570945016134,26.512426752707,-30.4190829565415));
#27596=CARTESIAN_POINT('Ctrl Pts',(-24.5661446532548,26.6243825795122,-30.4406920981083));
#27597=CARTESIAN_POINT('Ctrl Pts',(-24.2479013163498,26.6966259625061,-30.4613445472688));
#27598=CARTESIAN_POINT('Ctrl Pts',(-24.2320884196013,26.7000905340298,-30.4623628158075));
#27599=CARTESIAN_POINT('Ctrl Pts',(-24.2127426893788,26.7041766273685,-30.4635983697762));
#27600=CARTESIAN_POINT('Ctrl Pts',(-24.2092344245252,26.7049115109712,-30.4638220229564));
#27601=CARTESIAN_POINT('Ctrl Pts',(-24.2034488875219,26.7061133472418,-30.4641901703862));
#27602=CARTESIAN_POINT('Ctrl Pts',(-24.2011723359378,26.7065836890492,-30.4643348586425));
#27603=CARTESIAN_POINT('Ctrl Pts',(-24.1971080543292,26.7074187966109,-30.4645928544933));
#27604=CARTESIAN_POINT('Ctrl Pts',(-24.1953205273345,26.7077845065994,-30.464706216421));
#27605=CARTESIAN_POINT('Ctrl Pts',(-24.1917008116831,26.7085218618142,-30.4649355532503));
#27606=CARTESIAN_POINT('Ctrl Pts',(-24.189868616906,26.7088934294631,-30.4650515233761));
#27607=CARTESIAN_POINT('Ctrl Pts',(-24.184797483288,26.7099172580589,-30.4653721930844));
#27608=CARTESIAN_POINT('Ctrl Pts',(-24.1815578514779,26.7105661351317,-30.4655766975536));
#27609=CARTESIAN_POINT('Ctrl Pts',(-24.1744627206393,26.7119758981761,-30.4660238257275));
#27610=CARTESIAN_POINT('Ctrl Pts',(-24.1706068094036,26.7127347176761,-30.4662663318913));
#27611=CARTESIAN_POINT('Ctrl Pts',(-24.1592671837969,26.7149447485685,-30.4669780911508));
#27612=CARTESIAN_POINT('Ctrl Pts',(-24.151779633724,26.7163764746666,-30.4674462575447));
#27613=CARTESIAN_POINT('Ctrl Pts',(-23.8706312918523,26.7691026838073,-30.4849599311715));
#27614=CARTESIAN_POINT('Ctrl Pts',(-23.5914249828275,26.7847545344439,-30.5000963244803));
#27615=CARTESIAN_POINT('Ctrl Pts',(-23.2212777852796,26.7575053768555,-30.520917584913));
#27616=CARTESIAN_POINT('Ctrl Pts',(-23.129251950374,26.7467275321325,-30.5261491574218));
#27617=CARTESIAN_POINT('Ctrl Pts',(-23.0198448949343,26.7291071748471,-30.5325202795852));
#27618=CARTESIAN_POINT('Ctrl Pts',(-23.0018933449354,26.7260597189684,-30.5335705176079));
#27619=CARTESIAN_POINT('Ctrl Pts',(-22.9441085196505,26.7157456147818,-30.5369683054403));
#27620=CARTESIAN_POINT('Ctrl Pts',(-22.904387082252,26.7078805429485,-30.5393303430552));
#27621=CARTESIAN_POINT('Ctrl Pts',(-22.7936632030015,26.6837799593381,-30.5460008612745));
#27622=CARTESIAN_POINT('Ctrl Pts',(-22.7230511849288,26.6658838028677,-30.5503555532915));
#27623=CARTESIAN_POINT('Ctrl Pts',(-22.643480072533,26.6428213331935,-30.5553994666403));
#27624=CARTESIAN_POINT('Ctrl Pts',(-22.6338634750866,26.6399853968554,-30.55601133696));
#27625=CARTESIAN_POINT('Ctrl Pts',(-22.6199611895901,26.6358149970042,-30.5568992565498));
#27626=CARTESIAN_POINT('Ctrl Pts',(-22.6156647431757,26.6345163618087,-30.5571741311988));
#27627=CARTESIAN_POINT('Ctrl Pts',(-22.6081157370842,26.6322173923887,-30.5576579216964));
#27628=CARTESIAN_POINT('Ctrl Pts',(-22.6048620155102,26.6312208720186,-30.5578667120766));
#27629=CARTESIAN_POINT('Ctrl Pts',(-22.5981661591933,26.6291585202097,-30.5582969425794));
#27630=CARTESIAN_POINT('Ctrl Pts',(-22.5947242227068,26.6280920657462,-30.558518402933));
#27631=CARTESIAN_POINT('Ctrl Pts',(-22.585974182157,26.6253648485503,-30.5590821754393));
#27632=CARTESIAN_POINT('Ctrl Pts',(-22.5806685912022,26.6236961180295,-30.559424749439));
#27633=CARTESIAN_POINT('Ctrl Pts',(-22.5594669748747,26.6169673588041,-30.5607966490888));
#27634=CARTESIAN_POINT('Ctrl Pts',(-22.5436062447099,26.6117977439168,-30.561829582323));
#27635=CARTESIAN_POINT('Ctrl Pts',(-22.4422558208104,26.5778910734511,-30.5684733855978));
#27636=CARTESIAN_POINT('Ctrl Pts',(-22.3579716391042,26.5457016635174,-30.5741984001336));
#27637=CARTESIAN_POINT('Ctrl Pts',(-22.2073804094754,26.4808254844909,-30.5848078846483));
#27638=CARTESIAN_POINT('Ctrl Pts',(-22.1406353433465,26.4493111592343,-30.5896524661825));
#27639=CARTESIAN_POINT('Ctrl Pts',(-22.0750360141079,26.4155367739188,-30.5945512678406));
#27640=CARTESIAN_POINT('',(-26.7730022627907,23.5515690488782,-30.4357734492251));
#27641=CARTESIAN_POINT('Ctrl Pts',(-22.0750360153473,26.4155367745569,-30.8398067994259));
#27642=CARTESIAN_POINT('Ctrl Pts',(-22.0896415646513,26.4230565686636,-30.8388053845237));
#27643=CARTESIAN_POINT('Ctrl Pts',(-22.1043047924991,26.4304647802139,-30.8378104288188));
#27644=CARTESIAN_POINT('Ctrl Pts',(-22.1562909130468,26.4562323249972,-30.8343173602465));
#27645=CARTESIAN_POINT('Ctrl Pts',(-22.1939133292558,26.4739816325899,-30.8318515798414));
#27646=CARTESIAN_POINT('Ctrl Pts',(-22.271427038284,26.5087322291368,-30.8268761304353));
#27647=CARTESIAN_POINT('Ctrl Pts',(-22.3113387733486,26.5256667448064,-30.8243695128954));
#27648=CARTESIAN_POINT('Ctrl Pts',(-22.4738574150107,26.5907858705176,-30.8143381125657));
#27649=CARTESIAN_POINT('Ctrl Pts',(-22.5990278524788,26.6322395860278,-30.8070055666797));
#27650=CARTESIAN_POINT('Ctrl Pts',(-22.8937240215838,26.7101649942925,-30.7899699113415));
#27651=CARTESIAN_POINT('Ctrl Pts',(-23.0643419887723,26.7408575560767,-30.7802623955911));
#27652=CARTESIAN_POINT('Ctrl Pts',(-23.2645785093251,26.7604392800701,-30.7685091963496));
#27653=CARTESIAN_POINT('Ctrl Pts',(-23.2926045056041,26.7628100852407,-30.7668565829421));
#27654=CARTESIAN_POINT('Ctrl Pts',(-23.331741746087,26.7656054033468,-30.7645363181845));
#27655=CARTESIAN_POINT('Ctrl Pts',(-23.3428300446381,26.7663397444739,-30.7638775544502));
#27656=CARTESIAN_POINT('Ctrl Pts',(-23.407200966481,26.7702685337694,-30.7600447307454));
#27657=CARTESIAN_POINT('Ctrl Pts',(-23.4605500761491,26.7721960073218,-30.7568341862726));
#27658=CARTESIAN_POINT('Ctrl Pts',(-23.5226744088817,26.7728964239378,-30.7530481043858));
#27659=CARTESIAN_POINT('Ctrl Pts',(-23.5314289522968,26.772959449729,-30.7525134800927));
#27660=CARTESIAN_POINT('Ctrl Pts',(-23.5444762355346,26.7730002140307,-30.7517150453256));
#27661=CARTESIAN_POINT('Ctrl Pts',(-23.5487689006376,26.7730050490555,-30.7514520857702));
#27662=CARTESIAN_POINT('Ctrl Pts',(-23.5564247971283,26.7729983760178,-30.7509826194275));
#27663=CARTESIAN_POINT('Ctrl Pts',(-23.5597880312251,26.7729901797316,-30.7507762169138));
#27664=CARTESIAN_POINT('Ctrl Pts',(-23.5668781877368,26.7729618019281,-30.7503407396844));
#27665=CARTESIAN_POINT('Ctrl Pts',(-23.5706050980211,26.7729404200489,-30.7501116275816));
#27666=CARTESIAN_POINT('Ctrl Pts',(-23.5804479922134,26.772866874851,-30.7495059882894));
#27667=CARTESIAN_POINT('Ctrl Pts',(-23.5865638575088,26.7728037659414,-30.7491291179597));
#27668=CARTESIAN_POINT('Ctrl Pts',(-23.6142202505335,26.7724396428028,-30.747422331667));
#27669=CARTESIAN_POINT('Ctrl Pts',(-23.6357572087454,26.7719400649529,-30.7460861963887));
#27670=CARTESIAN_POINT('Ctrl Pts',(-23.793485220148,26.7666986802268,-30.7362477508896));
#27671=CARTESIAN_POINT('Ctrl Pts',(-23.9292405103811,26.7535394864115,-30.7274805953845));
#27672=CARTESIAN_POINT('Ctrl Pts',(-24.1033085259862,26.7254459097807,-30.7158523677548));
#27673=CARTESIAN_POINT('Ctrl Pts',(-24.1427522735887,26.7183225768443,-30.7131920352082));
#27674=CARTESIAN_POINT('Ctrl Pts',(-24.2128996231742,26.7042985062799,-30.7084186982923));
#27675=CARTESIAN_POINT('Ctrl Pts',(-24.2436548780747,26.6976801005883,-30.7063112961726));
#27676=CARTESIAN_POINT('Ctrl Pts',(-24.2996732027336,26.6847642680805,-30.7024483376437));
#27677=CARTESIAN_POINT('Ctrl Pts',(-24.3249665393735,26.6786088650635,-30.7006949379456));
#27678=CARTESIAN_POINT('Ctrl Pts',(-24.371673866749,26.6666409487333,-30.6974415540267));
#27679=CARTESIAN_POINT('Ctrl Pts',(-24.3931078930697,26.6609123660805,-30.6959424745147));
#27680=CARTESIAN_POINT('Ctrl Pts',(-24.4330530342956,26.6497932208371,-30.6931384441911));
#27681=CARTESIAN_POINT('Ctrl Pts',(-24.4515783206892,26.6444569577199,-30.6918338530952));
#27682=CARTESIAN_POINT('Ctrl Pts',(-24.4863444610054,26.6341037530824,-30.6893785057667));
#27683=CARTESIAN_POINT('Ctrl Pts',(-24.5025957205963,26.6291239006293,-30.6882278505086));
#27684=CARTESIAN_POINT('Ctrl Pts',(-24.6745433977778,26.5749425435578,-30.6760257244682));
#27685=CARTESIAN_POINT('Ctrl Pts',(-24.8263400034613,26.5140997215737,-30.6649999976738));
#27686=CARTESIAN_POINT('Ctrl Pts',(-25.008685592226,26.4243928804284,-30.6519102651671));
#27687=CARTESIAN_POINT('Ctrl Pts',(-25.0441613391181,26.4061143238229,-30.6493720376264));
#27688=CARTESIAN_POINT('Ctrl Pts',(-25.0839761424602,26.3846550758923,-30.6465406795878));
#27689=CARTESIAN_POINT('Ctrl Pts',(-25.0886556539219,26.3821179471519,-30.6462081795906));
#27690=CARTESIAN_POINT('Ctrl Pts',(-25.0954802137077,26.3783959117298,-30.645723690707));
#27691=CARTESIAN_POINT('Ctrl Pts',(-25.0976301994596,26.3772201510165,-30.6455711209473));
#27692=CARTESIAN_POINT('Ctrl Pts',(-25.1014328647216,26.3751349531954,-30.6453013844033));
#27693=CARTESIAN_POINT('Ctrl Pts',(-25.1030860878248,26.3742265166853,-30.6451841532012));
#27694=CARTESIAN_POINT('Ctrl Pts',(-25.1064994497403,26.3723469903577,-30.6449421884633));
#27695=CARTESIAN_POINT('Ctrl Pts',(-25.1082594737742,26.3713757073161,-30.6448174679982));
#27696=CARTESIAN_POINT('Ctrl Pts',(-25.1127694359319,26.3688813416591,-30.6444979868244));
#27697=CARTESIAN_POINT('Ctrl Pts',(-25.1155180646345,26.3673558766183,-30.6443033797757));
#27698=CARTESIAN_POINT('Ctrl Pts',(-25.1215271747893,26.3640093629202,-30.6438781415758));
#27699=CARTESIAN_POINT('Ctrl Pts',(-25.1247867371966,26.3621866606058,-30.6436476160705));
#27700=CARTESIAN_POINT('Ctrl Pts',(-25.1342395880614,26.356879166635,-30.6429794667181));
#27701=CARTESIAN_POINT('Ctrl Pts',(-25.1404245762917,26.3533795237318,-30.642542775759));
#27702=CARTESIAN_POINT('Ctrl Pts',(-25.1614114643989,26.3414127279415,-30.6410624502854));
#27703=CARTESIAN_POINT('Ctrl Pts',(-25.1761580135121,26.3328483953251,-30.6400247576722));
#27704=CARTESIAN_POINT('Ctrl Pts',(-25.2354706131042,26.2977689871749,-30.6358581440697));
#27705=CARTESIAN_POINT('Ctrl Pts',(-25.2794640673054,26.2702956878254,-30.6327840256834));
#27706=CARTESIAN_POINT('Ctrl Pts',(-25.3822358234883,26.202614360581,-30.6255948593987));
#27707=CARTESIAN_POINT('Ctrl Pts',(-25.4403831712318,26.161496158141,-30.6215208040603));
#27708=CARTESIAN_POINT('Ctrl Pts',(-25.7757914055035,25.9072368850689,-30.5976899544582));
#27709=CARTESIAN_POINT('Ctrl Pts',(-26.0181963368405,25.652073300597,-30.5787784602397));
#27710=CARTESIAN_POINT('Ctrl Pts',(-26.2263704658291,25.3460608378841,-30.5563966807607));
#27711=CARTESIAN_POINT('Ctrl Pts',(-26.2376968839226,25.3290660390078,-30.5551556795549));
#27712=CARTESIAN_POINT('Ctrl Pts',(-26.2522817390364,25.3067248166451,-30.5535264381184));
#27713=CARTESIAN_POINT('Ctrl Pts',(-26.2556873804691,25.3014746773092,-30.5531437251543));
#27714=CARTESIAN_POINT('Ctrl Pts',(-26.2609104028558,25.2933712631271,-30.552553246362));
#27715=CARTESIAN_POINT('Ctrl Pts',(-26.2627386323656,25.2905249701039,-30.5523458857275));
#27716=CARTESIAN_POINT('Ctrl Pts',(-26.2663646508542,25.2848601803131,-30.5519332719248));
#27717=CARTESIAN_POINT('Ctrl Pts',(-26.268162542628,25.282041754096,-30.5517280229265));
#27718=CARTESIAN_POINT('Ctrl Pts',(-26.272130102672,25.2758006976413,-30.551273611167));
#27719=CARTESIAN_POINT('Ctrl Pts',(-26.2742977047105,25.2723767663307,-30.5510243720673));
#27720=CARTESIAN_POINT('Ctrl Pts',(-26.2805089075306,25.2625245190747,-30.5503073544005));
#27721=CARTESIAN_POINT('Ctrl Pts',(-26.2845362312402,25.2560860186964,-30.5498389737924));
#27722=CARTESIAN_POINT('Ctrl Pts',(-26.3109358254074,25.2135471746394,-30.546745604233));
#27723=CARTESIAN_POINT('Ctrl Pts',(-26.3326144774095,25.1770232721595,-30.5440952171019));
#27724=CARTESIAN_POINT('Ctrl Pts',(-26.3942783487156,25.0682927778022,-30.5362166880143));
#27725=CARTESIAN_POINT('Ctrl Pts',(-26.4322164859861,24.9949707910128,-30.5309176222556));
#27726=CARTESIAN_POINT('Ctrl Pts',(-26.6041806500607,24.6288266619948,-30.5045205254442));
#27727=CARTESIAN_POINT('Ctrl Pts',(-26.6965903755075,24.3185668852515,-30.4821115131693));
#27728=CARTESIAN_POINT('Ctrl Pts',(-26.7431534170635,23.9880228588051,-30.4602696852952));
#27729=CARTESIAN_POINT('Ctrl Pts',(-26.7447467514788,23.9762403370877,-30.4594940394283));
#27730=CARTESIAN_POINT('Ctrl Pts',(-26.7464584706982,23.9630323747509,-30.4586280200418));
#27731=CARTESIAN_POINT('Ctrl Pts',(-26.7466411350313,23.9616155099008,-30.4585351636877));
#27732=CARTESIAN_POINT('Ctrl Pts',(-26.7475863015471,23.9542455360234,-30.4580523949869));
#27733=CARTESIAN_POINT('Ctrl Pts',(-26.7483331201726,23.9482903866946,-30.4576630965287));
#27734=CARTESIAN_POINT('Ctrl Pts',(-26.7492392382619,23.9408977734967,-30.4571808391253));
#27735=CARTESIAN_POINT('Ctrl Pts',(-26.7494142067891,23.939462282803,-30.4570872420964));
#27736=CARTESIAN_POINT('Ctrl Pts',(-26.7504927256297,23.9305639488393,-30.4565073467545));
#27737=CARTESIAN_POINT('Ctrl Pts',(-26.7513711365737,23.9230980124563,-30.4560220845911));
#27738=CARTESIAN_POINT('Ctrl Pts',(-26.7567164489198,23.8762544524727,-30.4529857364108));
#27739=CARTESIAN_POINT('Ctrl Pts',(-26.7604830691188,23.8367980929405,-30.4504651099382));
#27740=CARTESIAN_POINT('Ctrl Pts',(-26.7639283268978,23.7919831049697,-30.4476514652907));
#27741=CARTESIAN_POINT('Ctrl Pts',(-26.7643224524585,23.7866850424314,-30.447319614519));
#27742=CARTESIAN_POINT('Ctrl Pts',(-26.7648790846507,23.7789437706466,-30.4468358942514));
#27743=CARTESIAN_POINT('Ctrl Pts',(-26.7650519081915,23.7765013476353,-30.4466834464799));
#27744=CARTESIAN_POINT('Ctrl Pts',(-26.7653529280629,23.7721772059014,-30.4464138505772));
#27745=CARTESIAN_POINT('Ctrl Pts',(-26.7654822561327,23.7702955704694,-30.4462966382534));
#27746=CARTESIAN_POINT('Ctrl Pts',(-26.7657282010927,23.7666707248699,-30.4460710328125));
#27747=CARTESIAN_POINT('Ctrl Pts',(-26.7658450518867,23.7649275394335,-30.4459626265691));
#27748=CARTESIAN_POINT('Ctrl Pts',(-26.7660938256411,23.7611705429245,-30.4457291706014));
#27749=CARTESIAN_POINT('Ctrl Pts',(-26.766225274738,23.7591566995994,-30.4456041477784));
#27750=CARTESIAN_POINT('Ctrl Pts',(-26.7665386882908,23.7542846946977,-30.4453019616243));
#27751=CARTESIAN_POINT('Ctrl Pts',(-26.7667187350782,23.7514264049812,-30.4451249060969));
#27752=CARTESIAN_POINT('Ctrl Pts',(-26.7671964395218,23.7436781166658,-30.4446455557152));
#27753=CARTESIAN_POINT('Ctrl Pts',(-26.7674867590106,23.7387876487219,-30.4443436680854));
#27754=CARTESIAN_POINT('Ctrl Pts',(-26.7712280359402,23.6732390291014,-30.4403060186204));
#27755=CARTESIAN_POINT('Ctrl Pts',(-26.7729743898063,23.612491610421,-30.4366633785719));
#27756=CARTESIAN_POINT('Ctrl Pts',(-26.7730021943074,23.5517271931927,-30.4330867142687));
#27757=CARTESIAN_POINT('Ctrl Pts',(-26.7730022627907,23.5515690488782,-30.4357734492251));
#27758=CARTESIAN_POINT('Ctrl Pts',(-26.77304247429,23.4531338744264,-30.4296632602288));
#27759=CARTESIAN_POINT('Ctrl Pts',(-26.7685685722269,23.3545143288027,-30.4235530712325));
#27760=CARTESIAN_POINT('Ctrl Pts',(-26.7595561131448,23.2561639658024,-30.4174428822362));
#27761=CARTESIAN_POINT('Ctrl Pts',(-26.7505553265621,23.1579409814163,-30.4113406068599));
#27762=CARTESIAN_POINT('Ctrl Pts',(-26.7370277015207,23.0599869250309,-30.4052383314836));
#27763=CARTESIAN_POINT('Ctrl Pts',(-26.7190008029838,22.9627561864298,-30.3991360561074));
#27764=CARTESIAN_POINT('Ctrl Pts',(-26.7006986159141,22.8640406384855,-30.3929405929633));
#27765=CARTESIAN_POINT('Ctrl Pts',(-26.6777585735126,22.7660711481936,-30.3867451298192));
#27766=CARTESIAN_POINT('Ctrl Pts',(-26.6502643952142,22.6693189311685,-30.3805496666752));
#27767=CARTESIAN_POINT('Ctrl Pts',(-26.6232272244863,22.5741749271682,-30.3744571843705));
#27768=CARTESIAN_POINT('Ctrl Pts',(-26.5917862856016,22.4802084820841,-30.3683647020658));
#27769=CARTESIAN_POINT('Ctrl Pts',(-26.5560725534804,22.3878569195513,-30.3622722197611));
#27770=CARTESIAN_POINT('Ctrl Pts',(-26.5203688660586,22.2955313314444,-30.3561814510033));
#27771=CARTESIAN_POINT('Ctrl Pts',(-26.4803949324917,22.2048201373144,-30.3500906822455));
#27772=CARTESIAN_POINT('Ctrl Pts',(-26.4363308136407,22.1161431519826,-30.3439999134877));
#27773=CARTESIAN_POINT('Ctrl Pts',(-26.3922667373225,22.027466252246,-30.337909150609));
#27774=CARTESIAN_POINT('Ctrl Pts',(-26.3441126820331,21.940823954374,-30.3318183877303));
#27775=CARTESIAN_POINT('Ctrl Pts',(-26.2920953441146,21.8566127959538,-30.3257276248516));
#27776=CARTESIAN_POINT('Ctrl Pts',(-26.2385168775424,21.7698743176509,-30.3194540678348));
#27777=CARTESIAN_POINT('Ctrl Pts',(-26.1808398076691,21.6857156553139,-30.313180510818));
#27778=CARTESIAN_POINT('Ctrl Pts',(-26.11935980296,21.6045379094464,-30.3069069538011));
#27779=CARTESIAN_POINT('Ctrl Pts',(-26.0595866822292,21.525613920625,-30.3008075710383));
#27780=CARTESIAN_POINT('Ctrl Pts',(-25.9962193630557,21.4495078018546,-30.2947081882755));
#27781=CARTESIAN_POINT('Ctrl Pts',(-25.9295693813819,21.3765531754601,-30.2886088055127));
#27782=CARTESIAN_POINT('Ctrl Pts',(-25.8600645098058,21.3004736055775,-30.2822481613689));
#27783=CARTESIAN_POINT('Ctrl Pts',(-25.7869898592751,21.2278219288648,-30.275887517225));
#27784=CARTESIAN_POINT('Ctrl Pts',(-25.7107384781269,21.1589311317634,-30.2695268730812));
#27785=CARTESIAN_POINT('Ctrl Pts',(-25.6344870969787,21.0900403346621,-30.2631662289373));
#27786=CARTESIAN_POINT('Ctrl Pts',(-25.5550594510845,21.024910698303,-30.2568055847935));
#27787=CARTESIAN_POINT('Ctrl Pts',(-25.4728825618927,20.9638242358625,-30.2504449406496));
#27788=CARTESIAN_POINT('Ctrl Pts',(-25.3931416972281,20.9045486003132,-30.2442728493373));
#27789=CARTESIAN_POINT('Ctrl Pts',(-25.310516577792,20.8488596986913,-30.238100758025));
#27790=CARTESIAN_POINT('Ctrl Pts',(-25.2253636729472,20.7970507179962,-30.2319286667126));
#27791=CARTESIAN_POINT('Ctrl Pts',(-25.1403261418701,20.745311933348,-30.2257649379739));
#27792=CARTESIAN_POINT('Ctrl Pts',(-25.0527680005755,20.6974428447619,-30.2196012092351));
#27793=CARTESIAN_POINT('Ctrl Pts',(-24.963077241254,20.6536952816891,-30.2134374804963));
#27794=CARTESIAN_POINT('Ctrl Pts',(-24.8734815008737,20.6099940650533,-30.2072802816496));
#27795=CARTESIAN_POINT('Ctrl Pts',(-24.7817580224552,20.5704058825787,-30.2011230828029));
#27796=CARTESIAN_POINT('Ctrl Pts',(-24.6883212883984,20.5351377631466,-30.1949658839562));
#27797=CARTESIAN_POINT('Ctrl Pts',(-24.5949528509282,20.4998954225712,-30.1888131856485));
#27798=CARTESIAN_POINT('Ctrl Pts',(-24.4998740527622,20.4689670199309,-30.1826604873408));
#27799=CARTESIAN_POINT('Ctrl Pts',(-24.4035205023671,20.4425119806308,-30.1765077890331));
#27800=CARTESIAN_POINT('Ctrl Pts',(-24.3072034893753,20.4160669731193,-30.1703574238374));
#27801=CARTESIAN_POINT('Ctrl Pts',(-24.2096131030746,20.394092073292,-30.1642070586416));
#27802=CARTESIAN_POINT('Ctrl Pts',(-24.111200453139,20.3766969560147,-30.1580566934459));
#27803=CARTESIAN_POINT('Ctrl Pts',(-24.0127987931402,20.3593037812847,-30.1519070150737));
#27804=CARTESIAN_POINT('Ctrl Pts',(-23.9135754798358,20.346489447917,-30.1457573367014));
#27805=CARTESIAN_POINT('Ctrl Pts',(-23.8139911698563,20.3383123869779,-30.1396076583292));
#27806=CARTESIAN_POINT('Ctrl Pts',(-23.7143913391297,20.3301340516,-30.1334570214968));
#27807=CARTESIAN_POINT('Ctrl Pts',(-23.6144308329609,20.3265944597579,-30.1273063846643));
#27808=CARTESIAN_POINT('Ctrl Pts',(-23.5145737635325,20.3277000359228,-30.1211557478318));
#27809=CARTESIAN_POINT('Ctrl Pts',(-23.4146098680168,20.3288067948219,-30.11499853111));
#27810=CARTESIAN_POINT('Ctrl Pts',(-23.3147500654339,20.3345686402192,-30.1088413143882));
#27811=CARTESIAN_POINT('Ctrl Pts',(-23.2154566783019,20.3449398637862,-30.1026840976664));
#27812=CARTESIAN_POINT('Ctrl Pts',(-23.116107895796,20.3553168734164,-30.0965234458586));
#27813=CARTESIAN_POINT('Ctrl Pts',(-23.0173265875522,20.3703083172426,-30.0903627940508));
#27814=CARTESIAN_POINT('Ctrl Pts',(-22.919566093302,20.3898170903463,-30.084202142243));
#27815=CARTESIAN_POINT('Ctrl Pts',(-22.8216420109809,20.4093585085647,-30.0780311814739));
#27816=CARTESIAN_POINT('Ctrl Pts',(-22.7247425764993,20.433432250389,-30.0718602207049));
#27817=CARTESIAN_POINT('Ctrl Pts',(-22.6293072918812,20.4618909227232,-30.0656892599359));
#27818=CARTESIAN_POINT('Ctrl Pts',(-22.5564597472485,20.4836139616532,-30.0609788497155));
#27819=CARTESIAN_POINT('Ctrl Pts',(-22.4844650125374,20.5078908642717,-30.0562684394952));
#27820=CARTESIAN_POINT('Ctrl Pts',(-22.4135100480725,20.5346374885513,-30.0515580292748));
#27821=CARTESIAN_POINT('Ctrl Pts',(-22.3205371435372,20.5696838220186,-30.0453859379625));
#27822=CARTESIAN_POINT('Ctrl Pts',(-22.2290227564579,20.6090955091581,-30.0392138466501));
#27823=CARTESIAN_POINT('Ctrl Pts',(-22.1394062367787,20.6527311263163,-30.0330417553378));
#27824=CARTESIAN_POINT('Ctrl Pts',(-22.0499111386242,20.696307621527,-30.026878026599));
#27825=CARTESIAN_POINT('Ctrl Pts',(-21.9623091840145,20.7440964831748,-30.0207142978602));
#27826=CARTESIAN_POINT('Ctrl Pts',(-21.8770219675195,20.795907411414,-30.0145505691215));
#27827=CARTESIAN_POINT('Ctrl Pts',(-21.7918251048255,20.8476634508375,-30.0083933702748));
#27828=CARTESIAN_POINT('Ctrl Pts',(-21.70893847417,20.9034328613005,-30.0022361714281));
#27829=CARTESIAN_POINT('Ctrl Pts',(-21.6287602977326,20.9629788396923,-29.9960789725814));
#27830=CARTESIAN_POINT('Ctrl Pts',(-21.5486407266801,21.0224812935848,-29.9899262742737));
#27831=CARTESIAN_POINT('Ctrl Pts',(-21.4712260215294,21.0857545689622,-29.983773575966));
#27832=CARTESIAN_POINT('Ctrl Pts',(-21.3968857743915,21.152518357303,-29.9776208776583));
#27833=CARTESIAN_POINT('Ctrl Pts',(-21.3225737171811,21.2192568287201,-29.9714705124626));
#27834=CARTESIAN_POINT('Ctrl Pts',(-21.2513341243105,21.2894828931717,-29.9653201472668));
#27835=CARTESIAN_POINT('Ctrl Pts',(-21.1835031109869,21.3628763084345,-29.9591697820711));
#27836=CARTESIAN_POINT('Ctrl Pts',(-21.1156796724878,21.4362615277083,-29.9530201036988));
#27837=CARTESIAN_POINT('Ctrl Pts',(-21.0512643516077,21.5128130755611,-29.9468704253266));
#27838=CARTESIAN_POINT('Ctrl Pts',(-20.9905553118204,21.5921749783091,-29.9407207469544));
#27839=CARTESIAN_POINT('Ctrl Pts',(-20.9298368102049,21.6715492500337,-29.934570110122));
#27840=CARTESIAN_POINT('Ctrl Pts',(-20.8728260009893,21.7537344015906,-29.9284194732895));
#27841=CARTESIAN_POINT('Ctrl Pts',(-20.819779161499,21.8383434403127,-29.9222688364571));
#27842=CARTESIAN_POINT('Ctrl Pts',(-20.7666755730337,21.9230429929327,-29.9161116197353));
#27843=CARTESIAN_POINT('Ctrl Pts',(-20.7175446535865,22.0101712420173,-29.9099544030134));
#27844=CARTESIAN_POINT('Ctrl Pts',(-20.672597852894,22.0993145205857,-29.9037971862916));
#27845=CARTESIAN_POINT('Ctrl Pts',(-20.6276259765656,22.1885075318241,-29.8976365344838));
#27846=CARTESIAN_POINT('Ctrl Pts',(-20.5868430450439,22.2797174147473,-29.891475882676));
#27847=CARTESIAN_POINT('Ctrl Pts',(-20.5504124116753,22.3725102777079,-29.8853152308682));
#27848=CARTESIAN_POINT('Ctrl Pts',(-20.5139208169021,22.4654584161258,-29.8791442700992));
#27849=CARTESIAN_POINT('Ctrl Pts',(-20.481796207618,22.5599944141723,-29.8729733093301));
#27850=CARTESIAN_POINT('Ctrl Pts',(-20.4541521490144,22.6556688392038,-29.8668023485611));
#27851=CARTESIAN_POINT('Ctrl Pts',(-20.4330509200399,22.7286989242045,-29.8620919383407));
#27852=CARTESIAN_POINT('Ctrl Pts',(-20.4145592793517,22.8023919974991,-29.8573815281203));
#27853=CARTESIAN_POINT('Ctrl Pts',(-20.3987074968319,22.8765452838969,-29.8526711178999));
#27854=CARTESIAN_POINT('Ctrl Pts',(-20.3779367688915,22.9737089773633,-29.8464990265876));
#27855=CARTESIAN_POINT('Ctrl Pts',(-20.3616270767543,23.0720052543431,-29.8403269352752));
#27856=CARTESIAN_POINT('Ctrl Pts',(-20.3498969255981,23.1709880368763,-29.8341548439629));
#27857=CARTESIAN_POINT('Ctrl Pts',(-20.3381826676371,23.269836707525,-29.8279911152241));
#27858=CARTESIAN_POINT('Ctrl Pts',(-20.3310356685776,23.3693696073798,-29.8218273864853));
#27859=CARTESIAN_POINT('Ctrl Pts',(-20.3285237157046,23.4691291767217,-29.8156636577466));
#27860=CARTESIAN_POINT('Ctrl Pts',(-20.3260144240098,23.5687830601628,-29.8095064588999));
#27861=CARTESIAN_POINT('Ctrl Pts',(-20.3281304270622,23.6686627038138,-29.8033492600532));
#27862=CARTESIAN_POINT('Ctrl Pts',(-20.3348877544018,23.7683050745538,-29.7971920612065));
#27863=CARTESIAN_POINT('Ctrl Pts',(-20.3416401425449,23.8678746127632,-29.7910393628988));
#27864=CARTESIAN_POINT('Ctrl Pts',(-20.3530270807583,23.9672067907756,-29.7848866645911));
#27865=CARTESIAN_POINT('Ctrl Pts',(-20.369012520984,24.0658391459078,-29.7787339662834));
#27866=CARTESIAN_POINT('Ctrl Pts',(-20.3849918995079,24.1644340995105,-29.7725836010876));
#27867=CARTESIAN_POINT('Ctrl Pts',(-20.405566245794,24.2623293291983,-29.7664332358919));
#27868=CARTESIAN_POINT('Ctrl Pts',(-20.4306478192053,24.3590689511101,-29.7602828706961));
#27869=CARTESIAN_POINT('Ctrl Pts',(-20.4557265917072,24.4557977699156,-29.7541331923239));
#27870=CARTESIAN_POINT('Ctrl Pts',(-20.4853114816216,24.551370817013,-29.7479835139517));
#27871=CARTESIAN_POINT('Ctrl Pts',(-20.5192641723132,24.6453448236024,-29.7418338355795));
#27872=CARTESIAN_POINT('Ctrl Pts',(-20.5532221547131,24.7393334765431,-29.7356831987471));
#27873=CARTESIAN_POINT('Ctrl Pts',(-20.5915491424,24.8317221853703,-29.7295325619146));
#27874=CARTESIAN_POINT('Ctrl Pts',(-20.6340580807087,24.9220861537277,-29.7233819250821));
#27875=CARTESIAN_POINT('Ctrl Pts',(-20.6766124946516,25.0125467925487,-29.7172247083603));
#27876=CARTESIAN_POINT('Ctrl Pts',(-20.7233576076971,25.1009779716693,-29.7110674916385));
#27877=CARTESIAN_POINT('Ctrl Pts',(-20.7740596924203,25.1869781903385,-29.7049102749167));
#27878=CARTESIAN_POINT('Ctrl Pts',(-20.824790063629,25.2730263881774,-29.6987496231089));
#27879=CARTESIAN_POINT('Ctrl Pts',(-20.8794815650756,25.3566405611141,-29.692588971301));
#27880=CARTESIAN_POINT('Ctrl Pts',(-20.9378574558461,25.4374487404083,-29.6864283194932));
#27881=CARTESIAN_POINT('Ctrl Pts',(-20.9963310302405,25.5183921405221,-29.6802573587242));
#27882=CARTESIAN_POINT('Ctrl Pts',(-21.0585010383686,25.5965198279169,-29.6740863979551));
#27883=CARTESIAN_POINT('Ctrl Pts',(-21.1240507518066,25.6714933208953,-29.6679154371861));
#27884=CARTESIAN_POINT('Ctrl Pts',(-21.174086078829,25.7287219957807,-29.6632050269657));
#27885=CARTESIAN_POINT('Ctrl Pts',(-21.2260897821239,25.7841135535356,-29.6584946167454));
#27886=CARTESIAN_POINT('Ctrl Pts',(-21.2799076256754,25.8375329190133,-29.653784206525));
#27887=CARTESIAN_POINT('Ctrl Pts',(-21.3504158686518,25.9075191048615,-29.6476129680208));
#27888=CARTESIAN_POINT('Ctrl Pts',(-21.4242874215632,25.9743652245237,-29.6414417295167));
#27889=CARTESIAN_POINT('Ctrl Pts',(-21.5012111803779,26.0377305925212,-29.6352704910125));
#27890=CARTESIAN_POINT('Ctrl Pts',(-21.5780433761809,26.1010205361762,-29.6291065981866));
#27891=CARTESIAN_POINT('Ctrl Pts',(-21.6579202304885,26.1608376828121,-29.6229427053607));
#27892=CARTESIAN_POINT('Ctrl Pts',(-21.7404934092444,26.2168776424305,-29.6167788125348));
#27893=CARTESIAN_POINT('Ctrl Pts',(-21.8229734022357,26.2728543596432,-29.6106218758062));
#27894=CARTESIAN_POINT('Ctrl Pts',(-21.9081433105631,26.3250621247924,-29.6044649390776));
#27895=CARTESIAN_POINT('Ctrl Pts',(-21.9956222941264,26.3732371910468,-29.598308002349));
#27896=CARTESIAN_POINT('Ctrl Pts',(-22.021889173106,26.387702478406,-29.5964592896028));
#27897=CARTESIAN_POINT('Ctrl Pts',(-22.0483640244497,26.4018044680348,-29.5946105768567));
#27898=CARTESIAN_POINT('Ctrl Pts',(-22.0750360153461,26.4155367745563,-29.5927618641105));
#27899=CARTESIAN_POINT('Origin',(-23.5502525316942,23.5502525316942,-77.3107734492734));
#27900=CARTESIAN_POINT('',(-22.0750360120315,26.4155367728497,-28.0986394360247));
#27901=CARTESIAN_POINT('',(-22.0750360250495,26.4155367795522,-28.3456357132216));
#27902=CARTESIAN_POINT('',(-22.0750360153461,26.4155367745563,-77.3107734492734));
#27903=CARTESIAN_POINT('',(-26.7730017233255,23.5479699147772,-28.9373019452253));
#27904=CARTESIAN_POINT('Ctrl Pts',(-22.0750360120315,26.4155367728497,-28.0986394360247));
#27905=CARTESIAN_POINT('Ctrl Pts',(-22.0457737676643,26.4004708517544,-28.1005328265967));
#27906=CARTESIAN_POINT('Ctrl Pts',(-22.0167408821415,26.3849559218225,-28.1024119499114));
#27907=CARTESIAN_POINT('Ctrl Pts',(-21.6748533170991,26.1954628496327,-28.1246044605303));
#27908=CARTESIAN_POINT('Ctrl Pts',(-21.3928839179396,25.9710015176139,-28.1438902681475));
#27909=CARTESIAN_POINT('Ctrl Pts',(-21.1398241737672,25.6894988982981,-28.1667794881155));
#27910=CARTESIAN_POINT('Ctrl Pts',(-21.1262321418025,25.6740851533254,-28.1680281683821));
#27911=CARTESIAN_POINT('Ctrl Pts',(-21.108684928598,25.6537982414884,-28.1696660787883));
#27912=CARTESIAN_POINT('Ctrl Pts',(-21.1045950464036,25.6490417963526,-28.170049708029));
#27913=CARTESIAN_POINT('Ctrl Pts',(-21.0983191428002,25.6416998015274,-28.1706412827738));
#27914=CARTESIAN_POINT('Ctrl Pts',(-21.0961232492827,25.6391226787204,-28.170848820618));
#27915=CARTESIAN_POINT('Ctrl Pts',(-21.091788234588,25.6340187908414,-28.1712596231423));
#27916=CARTESIAN_POINT('Ctrl Pts',(-21.0896489373911,25.6314921801919,-28.1714628802191));
#27917=CARTESIAN_POINT('Ctrl Pts',(-21.0849647354103,25.62594259982,-28.1719090968935));
#27918=CARTESIAN_POINT('Ctrl Pts',(-21.0824214924024,25.6229182400776,-28.172152124204));
#27919=CARTESIAN_POINT('Ctrl Pts',(-21.0752520114677,25.6143605732085,-28.1728393777775));
#27920=CARTESIAN_POINT('Ctrl Pts',(-21.0706387987971,25.6088164283073,-28.1732841353436));
#27921=CARTESIAN_POINT('Ctrl Pts',(-21.060349706979,25.5963662613294,-28.1742818439563));
#27922=CARTESIAN_POINT('Ctrl Pts',(-21.0546838890198,25.5894520359693,-28.1748351998737));
#27923=CARTESIAN_POINT('Ctrl Pts',(-20.940071239815,25.448392557348,-28.1861101217549));
#27924=CARTESIAN_POINT('Ctrl Pts',(-20.8420786467419,25.3057463143876,-28.1972739626629));
#27925=CARTESIAN_POINT('Ctrl Pts',(-20.5967514026887,24.878826739896,-28.2300056570019));
#27926=CARTESIAN_POINT('Ctrl Pts',(-20.4796206664047,24.5795689191511,-28.2523197625039));
#27927=CARTESIAN_POINT('Ctrl Pts',(-20.40481865564,24.2521269563646,-28.2735771100213));
#27928=CARTESIAN_POINT('Ctrl Pts',(-20.4013172076754,24.2362469400368,-28.2746000397125));
#27929=CARTESIAN_POINT('Ctrl Pts',(-20.3971895140062,24.2168289031897,-28.2758405644299));
#27930=CARTESIAN_POINT('Ctrl Pts',(-20.3964488736767,24.2133158314876,-28.2760645865919));
#27931=CARTESIAN_POINT('Ctrl Pts',(-20.3952379829243,24.2075242958414,-28.2764332167125));
#27932=CARTESIAN_POINT('Ctrl Pts',(-20.394764328944,24.2052465601175,-28.2765780195515));
#27933=CARTESIAN_POINT('Ctrl Pts',(-20.3939150078018,24.2011399900831,-28.2768387700104));
#27934=CARTESIAN_POINT('Ctrl Pts',(-20.3935384643245,24.199311346555,-28.2769547679846));
#27935=CARTESIAN_POINT('Ctrl Pts',(-20.3927324527901,24.1953797444401,-28.2772039206444));
#27936=CARTESIAN_POINT('Ctrl Pts',(-20.3923034976272,24.1932766895667,-28.277337045227));
#27937=CARTESIAN_POINT('Ctrl Pts',(-20.3911351383668,24.1875191630919,-28.2777010940057));
#27938=CARTESIAN_POINT('Ctrl Pts',(-20.390399971814,24.1838638198422,-28.2779317741339));
#27939=CARTESIAN_POINT('Ctrl Pts',(-20.3866241110558,24.164919733748,-28.2791250121446));
#27940=CARTESIAN_POINT('Ctrl Pts',(-20.3836879595922,24.1496100101691,-28.2800816458943));
#27941=CARTESIAN_POINT('Ctrl Pts',(-20.3688848404305,24.0692766066483,-28.2850639507176));
#27942=CARTESIAN_POINT('Ctrl Pts',(-20.3589083696421,24.0039156259955,-28.288989741447));
#27943=CARTESIAN_POINT('Ctrl Pts',(-20.3414055106743,23.8596071438143,-28.2974681633333));
#27944=CARTESIAN_POINT('Ctrl Pts',(-20.3347676558959,23.7805954683339,-28.3019873584115));
#27945=CARTESIAN_POINT('Ctrl Pts',(-20.3176104769489,23.415212041599,-28.3226327839373));
#27946=CARTESIAN_POINT('Ctrl Pts',(-20.3423956066103,23.1285168796791,-28.3382485084046));
#27947=CARTESIAN_POINT('Ctrl Pts',(-20.4061312790621,22.8426796651111,-28.3555398922522));
#27948=CARTESIAN_POINT('Ctrl Pts',(-20.407530293231,22.8364915465942,-28.3559150095668));
#27949=CARTESIAN_POINT('Ctrl Pts',(-20.4098390087808,22.8264180262352,-28.3565269417755));
#27950=CARTESIAN_POINT('Ctrl Pts',(-20.4107376743249,22.8225300939839,-28.3567634329744));
#27951=CARTESIAN_POINT('Ctrl Pts',(-20.4131624841209,22.812127634291,-28.3573970294207));
#27952=CARTESIAN_POINT('Ctrl Pts',(-20.4147016935437,22.8056161968533,-28.3577945193885));
#27953=CARTESIAN_POINT('Ctrl Pts',(-20.4178650969972,22.7924175376324,-28.3586020675221));
#27954=CARTESIAN_POINT('Ctrl Pts',(-20.4194904543843,22.7857306330608,-28.3590121587173));
#27955=CARTESIAN_POINT('Ctrl Pts',(-20.4318543410835,22.7355648507611,-28.3620960318187));
#27956=CARTESIAN_POINT('Ctrl Pts',(-20.4434762945637,22.6923105764136,-28.3647965182208));
#27957=CARTESIAN_POINT('Ctrl Pts',(-20.458080002252,22.6421543994694,-28.3679810907144));
#27958=CARTESIAN_POINT('Ctrl Pts',(-20.4601894839292,22.6350020037225,-28.3684364875575));
#27959=CARTESIAN_POINT('Ctrl Pts',(-20.4635945384035,22.6236028091302,-28.3691643299522));
#27960=CARTESIAN_POINT('Ctrl Pts',(-20.4648741054659,22.6193512251498,-28.3694362509177));
#27961=CARTESIAN_POINT('Ctrl Pts',(-20.4671475010851,22.6118536522862,-28.3699165875322));
#27962=CARTESIAN_POINT('Ctrl Pts',(-20.4681376822445,22.6086065571885,-28.3701248832217));
#27963=CARTESIAN_POINT('Ctrl Pts',(-20.4701735865106,22.6019678431212,-28.3705512976928));
#27964=CARTESIAN_POINT('Ctrl Pts',(-20.4712197852755,22.5985763759219,-28.3707694318627));
#27965=CARTESIAN_POINT('Ctrl Pts',(-20.4737868247455,22.5903033355186,-28.3713022658019));
#27966=CARTESIAN_POINT('Ctrl Pts',(-20.4753136806577,22.5854236519577,-28.3716171631319));
#27967=CARTESIAN_POINT('Ctrl Pts',(-20.481322679037,22.5663786226375,-28.3728486068638));
#27968=CARTESIAN_POINT('Ctrl Pts',(-20.4858910908008,22.5522408798928,-28.3737679923199));
#27969=CARTESIAN_POINT('Ctrl Pts',(-20.497417591397,22.5173955230455,-28.3760472034784));
#27970=CARTESIAN_POINT('Ctrl Pts',(-20.5044887021416,22.4967263432852,-28.3774107401984));
#27971=CARTESIAN_POINT('Ctrl Pts',(-20.532596483792,22.4172148300085,-28.3827017580308));
#27972=CARTESIAN_POINT('Ctrl Pts',(-20.55513161223,22.3589203926956,-28.3866784342014));
#27973=CARTESIAN_POINT('Ctrl Pts',(-20.6410761734975,22.1544790325411,-28.4009806201322));
#27974=CARTESIAN_POINT('Ctrl Pts',(-20.7136011081862,22.012433146819,-28.4115913252341));
#27975=CARTESIAN_POINT('Ctrl Pts',(-20.9252502708133,21.6642252786945,-28.4390916016061));
#27976=CARTESIAN_POINT('Ctrl Pts',(-21.0782666922542,21.4676958156449,-28.4561251040388));
#27977=CARTESIAN_POINT('Ctrl Pts',(-21.2625359049252,21.2803006108625,-28.4727335983485));
#27978=CARTESIAN_POINT('Ctrl Pts',(-21.2728034451685,21.2699993078989,-28.4736476745489));
#27979=CARTESIAN_POINT('Ctrl Pts',(-21.285829001022,21.2571066696766,-28.474792652779));
#27980=CARTESIAN_POINT('Ctrl Pts',(-21.288522101492,21.2544504208411,-28.4750286027276));
#27981=CARTESIAN_POINT('Ctrl Pts',(-21.2927753915277,21.2502700793659,-28.4754000079284));
#27982=CARTESIAN_POINT('Ctrl Pts',(-21.2943324513777,21.2487428291979,-28.4755357128491));
#27983=CARTESIAN_POINT('Ctrl Pts',(-21.2972105638743,21.2459255446815,-28.475786071016));
#27984=CARTESIAN_POINT('Ctrl Pts',(-21.2985311669445,21.2446350726616,-28.475900758895));
#27985=CARTESIAN_POINT('Ctrl Pts',(-21.3014803658126,21.241758113757,-28.4761564652177));
#27986=CARTESIAN_POINT('Ctrl Pts',(-21.3031095279273,21.2401722187204,-28.476297436621));
#27987=CARTESIAN_POINT('Ctrl Pts',(-21.3078344902041,21.2355824695181,-28.4767054737042));
#27988=CARTESIAN_POINT('Ctrl Pts',(-21.3109346600731,21.232583090232,-28.476972187209));
#27989=CARTESIAN_POINT('Ctrl Pts',(-21.3322816495003,21.2120129364058,-28.4788018597472));
#27990=CARTESIAN_POINT('Ctrl Pts',(-21.3507297219677,21.1946509641895,-28.4803487599328));
#27991=CARTESIAN_POINT('Ctrl Pts',(-21.4080343618453,21.1419803023754,-28.4850568093903));
#27992=CARTESIAN_POINT('Ctrl Pts',(-21.4475522187311,21.1074005328722,-28.4881693969901));
#27993=CARTESIAN_POINT('Ctrl Pts',(-21.6076210183211,20.9740976309633,-28.5003382679784));
#27994=CARTESIAN_POINT('Ctrl Pts',(-21.734424714907,20.8832001422886,-28.5090316179169));
#27995=CARTESIAN_POINT('Ctrl Pts',(-22.0235578813535,20.7061558996501,-28.5279753231044));
#27996=CARTESIAN_POINT('Ctrl Pts',(-22.1876604078382,20.6239890641521,-28.5382073089231));
#27997=CARTESIAN_POINT('Ctrl Pts',(-22.4460779480476,20.5210718888121,-28.5544251766118));
#27998=CARTESIAN_POINT('Ctrl Pts',(-22.5358107410767,20.4898535339552,-28.5600698241396));
#27999=CARTESIAN_POINT('Ctrl Pts',(-22.6366378218943,20.4596973238734,-28.5664760012072));
#28000=CARTESIAN_POINT('Ctrl Pts',(-22.6465048792214,20.4567975849806,-28.5671035574248));
#28001=CARTESIAN_POINT('Ctrl Pts',(-22.6603503177924,20.4528005721681,-28.5679850933276));
#28002=CARTESIAN_POINT('Ctrl Pts',(-22.6643172574638,20.451663613897,-28.5682377764442));
#28003=CARTESIAN_POINT('Ctrl Pts',(-22.6715830818834,20.4495962610382,-28.5687007930918));
#28004=CARTESIAN_POINT('Ctrl Pts',(-22.6748812929801,20.4486635026506,-28.5689110492092));
#28005=CARTESIAN_POINT('Ctrl Pts',(-22.6812116091347,20.4468841443079,-28.5693147471649));
#28006=CARTESIAN_POINT('Ctrl Pts',(-22.6842434799975,20.4460367216741,-28.5695081618755));
#28007=CARTESIAN_POINT('Ctrl Pts',(-22.6918359285543,20.443926584322,-28.5699926803283));
#28008=CARTESIAN_POINT('Ctrl Pts',(-22.6963980438696,20.4426694726105,-28.5702839661719));
#28009=CARTESIAN_POINT('Ctrl Pts',(-22.7117232073031,20.4384828486854,-28.5712629763721));
#28010=CARTESIAN_POINT('Ctrl Pts',(-22.7224986013104,20.435599194055,-28.5719521897182));
#28011=CARTESIAN_POINT('Ctrl Pts',(-22.7480732931222,20.4288971163325,-28.5735901035087));
#28012=CARTESIAN_POINT('Ctrl Pts',(-22.762885109827,20.4251279438093,-28.5745403868792));
#28013=CARTESIAN_POINT('Ctrl Pts',(-22.8152588299014,20.4121963408617,-28.5779067108225));
#28014=CARTESIAN_POINT('Ctrl Pts',(-22.8529570386473,20.4036049212294,-28.5803409959292));
#28015=CARTESIAN_POINT('Ctrl Pts',(-22.9717341059481,20.3787748510699,-28.5880485090311));
#28016=CARTESIAN_POINT('Ctrl Pts',(-23.0532837118726,20.3649779230921,-28.5933960546017));
#28017=CARTESIAN_POINT('Ctrl Pts',(-23.2243120047308,20.3427702129441,-28.6047206496569));
#28018=CARTESIAN_POINT('Ctrl Pts',(-23.3137948937588,20.3349351179556,-28.6107075828226));
#28019=CARTESIAN_POINT('Ctrl Pts',(-23.651213964546,20.3195525459553,-28.6334266896517));
#28020=CARTESIAN_POINT('Ctrl Pts',(-23.8994266878082,20.33688921321,-28.6504978698463));
#28021=CARTESIAN_POINT('Ctrl Pts',(-24.1774287343905,20.3889268521848,-28.6686534037139));
#28022=CARTESIAN_POINT('Ctrl Pts',(-24.2115506383187,20.39588807887,-28.6708634308689));
#28023=CARTESIAN_POINT('Ctrl Pts',(-24.2500539190637,20.404395444659,-28.6733312249766));
#28024=CARTESIAN_POINT('Ctrl Pts',(-24.2545510434342,20.4053992122527,-28.6736190557927));
#28025=CARTESIAN_POINT('Ctrl Pts',(-24.2613561901461,20.4069334646038,-28.6740539798745));
#28026=CARTESIAN_POINT('Ctrl Pts',(-24.2636657819565,20.4074568487017,-28.6742014787334));
#28027=CARTESIAN_POINT('Ctrl Pts',(-24.2676825072062,20.408371747787,-28.6744578080761));
#28028=CARTESIAN_POINT('Ctrl Pts',(-24.2693898981495,20.4087621086226,-28.6745667053214));
#28029=CARTESIAN_POINT('Ctrl Pts',(-24.2729648554991,20.4095825184256,-28.6747945872698));
#28030=CARTESIAN_POINT('Ctrl Pts',(-24.2748323556039,20.4100128411563,-28.6749135554974));
#28031=CARTESIAN_POINT('Ctrl Pts',(-24.279301046538,20.4110467474254,-28.6751980574347));
#28032=CARTESIAN_POINT('Ctrl Pts',(-24.281901880967,20.4116519003913,-28.6753635000455));
#28033=CARTESIAN_POINT('Ctrl Pts',(-24.2907291271696,20.4137173613854,-28.675924543295));
#28034=CARTESIAN_POINT('Ctrl Pts',(-24.2969519949127,20.4151929826077,-28.6763192630331));
#28035=CARTESIAN_POINT('Ctrl Pts',(-24.3117396132708,20.4187460801285,-28.6772554492345));
#28036=CARTESIAN_POINT('Ctrl Pts',(-24.3203003678685,20.4208401961633,-28.6777959817824));
#28037=CARTESIAN_POINT('Ctrl Pts',(-24.4212888938915,20.4459833202594,-28.6841566350594));
#28038=CARTESIAN_POINT('Ctrl Pts',(-24.5126695466553,20.4730867865112,-28.6897556859943));
#28039=CARTESIAN_POINT('Ctrl Pts',(-24.7260409289243,20.5468108767779,-28.7027445753374));
#28040=CARTESIAN_POINT('Ctrl Pts',(-24.8466632624847,20.596870925378,-28.7100224867177));
#28041=CARTESIAN_POINT('Ctrl Pts',(-25.0222118266607,20.6825600099545,-28.7209374163615));
#28042=CARTESIAN_POINT('Ctrl Pts',(-25.0796271686613,20.712764624056,-28.7245613534846));
#28043=CARTESIAN_POINT('Ctrl Pts',(-25.2137529162196,20.7885786949616,-28.7332265286045));
#28044=CARTESIAN_POINT('Ctrl Pts',(-25.2895548991831,20.8356803928689,-28.738285974307));
#28045=CARTESIAN_POINT('Ctrl Pts',(-25.4617414420578,20.9528490235168,-28.7503097824543));
#28046=CARTESIAN_POINT('Ctrl Pts',(-25.5563820560106,21.0252309277073,-28.7573375949468));
#28047=CARTESIAN_POINT('Ctrl Pts',(-25.6548829332698,21.1096046956223,-28.7652293067485));
#28048=CARTESIAN_POINT('Ctrl Pts',(-25.6629368686961,21.1165730386487,-28.7658789716184));
#28049=CARTESIAN_POINT('Ctrl Pts',(-25.6741934702381,21.1264103467309,-28.7667932378602));
#28050=CARTESIAN_POINT('Ctrl Pts',(-25.6774252222514,21.1292460483723,-28.7670564522302));
#28051=CARTESIAN_POINT('Ctrl Pts',(-25.6830214968313,21.1341763569442,-28.7675135214894));
#28052=CARTESIAN_POINT('Ctrl Pts',(-25.6853886381995,21.1362679941637,-28.7677072519067));
#28053=CARTESIAN_POINT('Ctrl Pts',(-25.6901450071799,21.1404832535143,-28.7680973218956));
#28054=CARTESIAN_POINT('Ctrl Pts',(-25.6925341575451,21.1426069564222,-28.7682936647256));
#28055=CARTESIAN_POINT('Ctrl Pts',(-25.6973962959695,21.1469418520064,-28.7686940759141));
#28056=CARTESIAN_POINT('Ctrl Pts',(-25.6998690367107,21.1491533149193,-28.7688981555311));
#28057=CARTESIAN_POINT('Ctrl Pts',(-25.7055712828378,21.1542689117148,-28.7693697970876));
#28058=CARTESIAN_POINT('Ctrl Pts',(-25.708798335423,21.1571757591795,-28.7696374736355));
#28059=CARTESIAN_POINT('Ctrl Pts',(-25.7260470158395,21.1727762101977,-28.7710723125631));
#28060=CARTESIAN_POINT('Ctrl Pts',(-25.7399623349701,21.1855863291616,-28.7722444173748));
#28061=CARTESIAN_POINT('Ctrl Pts',(-25.8184708034618,21.259146629123,-28.778941702782));
#28062=CARTESIAN_POINT('Ctrl Pts',(-25.8806422236163,21.3224146156167,-28.7845758035015));
#28063=CARTESIAN_POINT('Ctrl Pts',(-25.9834335687823,21.4360350660689,-28.794494905584));
#28064=CARTESIAN_POINT('Ctrl Pts',(-26.0252946668328,21.4851977972338,-28.7987276692833));
#28065=CARTESIAN_POINT('Ctrl Pts',(-26.2620045503497,21.7807395581866,-28.8238093022325));
#28066=CARTESIAN_POINT('Ctrl Pts',(-26.4214492098276,22.0532594467184,-28.8457136511841));
#28067=CARTESIAN_POINT('Ctrl Pts',(-26.5415064264269,22.3508509004986,-28.8662754692804));
#28068=CARTESIAN_POINT('Ctrl Pts',(-26.5440395804668,22.3571878880069,-28.8667117733235));
#28069=CARTESIAN_POINT('Ctrl Pts',(-26.5560983834144,22.3876346694204,-28.8688004823148));
#28070=CARTESIAN_POINT('Ctrl Pts',(-26.5653533788868,22.4118516517457,-28.8704391043862));
#28071=CARTESIAN_POINT('Ctrl Pts',(-26.5759117200941,22.4405114090173,-28.8723494948835));
#28072=CARTESIAN_POINT('Ctrl Pts',(-26.5774986402483,22.4448476816115,-28.8726377669867));
#28073=CARTESIAN_POINT('Ctrl Pts',(-26.5798854598636,22.4514133747103,-28.8730730637447));
#28074=CARTESIAN_POINT('Ctrl Pts',(-26.5806922216405,22.4536402674668,-28.8732204977814));
#28075=CARTESIAN_POINT('Ctrl Pts',(-26.5821317838291,22.4576275903347,-28.8734841119724));
#28076=CARTESIAN_POINT('Ctrl Pts',(-26.5827655055024,22.4593876794983,-28.8736003474431));
#28077=CARTESIAN_POINT('Ctrl Pts',(-26.5841134085846,22.4631415771758,-28.8738479766281));
#28078=CARTESIAN_POINT('Ctrl Pts',(-26.5848271553455,22.4651355327885,-28.8739793438489));
#28079=CARTESIAN_POINT('Ctrl Pts',(-26.5867490358632,22.4705213120552,-28.8743337297367));
#28080=CARTESIAN_POINT('Ctrl Pts',(-26.5879534563827,22.4739144719093,-28.8745565256626));
#28081=CARTESIAN_POINT('Ctrl Pts',(-26.5938300578524,22.4905587898351,-28.8756471023783));
#28082=CARTESIAN_POINT('Ctrl Pts',(-26.5984213256531,22.5038386533231,-28.8765101090521));
#28083=CARTESIAN_POINT('Ctrl Pts',(-26.636521800248,22.6164200410221,-28.8837696013276));
#28084=CARTESIAN_POINT('Ctrl Pts',(-26.6652594053402,22.7172829949885,-28.8899018075406));
#28085=CARTESIAN_POINT('Ctrl Pts',(-26.744656370487,23.0582574373607,-28.9099530865801));
#28086=CARTESIAN_POINT('Ctrl Pts',(-26.7728280024169,23.3026992723123,-28.923287335281));
#28087=CARTESIAN_POINT('Ctrl Pts',(-26.7730017233255,23.5479699147772,-28.9373019452253));
#28088=CARTESIAN_POINT('Ctrl Pts',(-26.7730017261855,23.5479739563721,-28.9373021761595));
#28089=CARTESIAN_POINT('Ctrl Pts',(-26.77310750083,23.6975784688127,-28.9458504874898));
#28090=CARTESIAN_POINT('Ctrl Pts',(-26.7627962705988,23.8469938290537,-28.95460972371));
#28091=CARTESIAN_POINT('Ctrl Pts',(-26.741199785725,24.0019385244878,-28.9641350168917));
#28092=CARTESIAN_POINT('Ctrl Pts',(-26.7402311793074,24.0087291840131,-28.9645533451948));
#28093=CARTESIAN_POINT('Ctrl Pts',(-26.7386138167336,24.0198148236502,-28.9652376989888));
#28094=CARTESIAN_POINT('Ctrl Pts',(-26.7379780403255,24.0241116999024,-28.9655033132474));
#28095=CARTESIAN_POINT('Ctrl Pts',(-26.7368413629611,24.031688081907,-28.9659722812069));
#28096=CARTESIAN_POINT('Ctrl Pts',(-26.7363440803388,24.0349681308747,-28.9661755199251));
#28097=CARTESIAN_POINT('Ctrl Pts',(-26.7353577173884,24.0414070247902,-28.9665748982821));
#28098=CARTESIAN_POINT('Ctrl Pts',(-26.7348690002649,24.0445659221799,-28.9667710261764));
#28099=CARTESIAN_POINT('Ctrl Pts',(-26.7338880026587,24.05084490862,-28.9671612610362));
#28100=CARTESIAN_POINT('Ctrl Pts',(-26.7333958330707,24.0539650117883,-28.9673553642859));
#28101=CARTESIAN_POINT('Ctrl Pts',(-26.7322230130486,24.0613297258003,-28.967813980105));
#28102=CARTESIAN_POINT('Ctrl Pts',(-26.7315384563999,24.0655737010028,-28.9680786166914));
#28103=CARTESIAN_POINT('Ctrl Pts',(-26.7291290238785,24.0803234289836,-28.9689995929475));
#28104=CARTESIAN_POINT('Ctrl Pts',(-26.7273605963087,24.0908219075442,-28.9696573173102));
#28105=CARTESIAN_POINT('Ctrl Pts',(-26.7052103282031,24.2184552440559,-28.9776806382628));
#28106=CARTESIAN_POINT('Ctrl Pts',(-26.6784160768633,24.3343701443852,-28.9852512008797));
#28107=CARTESIAN_POINT('Ctrl Pts',(-26.6409941573877,24.4633081625523,-28.9940089287639));
#28108=CARTESIAN_POINT('Ctrl Pts',(-26.6365990521609,24.4780561349063,-28.9950156244242));
#28109=CARTESIAN_POINT('Ctrl Pts',(-26.6264426625231,24.5112654569427,-28.9972936394615));
#28110=CARTESIAN_POINT('Ctrl Pts',(-26.6206205161857,24.5297074730995,-28.9985665023647));
#28111=CARTESIAN_POINT('Ctrl Pts',(-26.528013106308,24.814105188315,-29.0183145735201));
#28112=CARTESIAN_POINT('Ctrl Pts',(-26.4071385078111,25.0676723411625,-29.0376800869498));
#28113=CARTESIAN_POINT('Ctrl Pts',(-26.2177285793629,25.3600599865555,-29.0605674288933));
#28114=CARTESIAN_POINT('Ctrl Pts',(-26.1785644887213,25.4164811813935,-29.0650052950319));
#28115=CARTESIAN_POINT('Ctrl Pts',(-26.1310546949927,25.4804595640769,-29.0700239003928));
#28116=CARTESIAN_POINT('Ctrl Pts',(-26.1244395149726,25.4892730002468,-29.0707149285074));
#28117=CARTESIAN_POINT('Ctrl Pts',(-26.1157831302581,25.5006835653382,-29.0716089842846));
#28118=CARTESIAN_POINT('Ctrl Pts',(-26.1137830614142,25.5033115918857,-29.0718148570516));
#28119=CARTESIAN_POINT('Ctrl Pts',(-26.1105342614802,25.5075668226656,-29.0721481264205));
#28120=CARTESIAN_POINT('Ctrl Pts',(-26.1092880169629,25.5091959088007,-29.0722756986184));
#28121=CARTESIAN_POINT('Ctrl Pts',(-26.1068926580093,25.5123209263377,-29.0725203799484));
#28122=CARTESIAN_POINT('Ctrl Pts',(-26.1057437888333,25.5138170341852,-29.0726375055454));
#28123=CARTESIAN_POINT('Ctrl Pts',(-26.1030992701564,25.5172545903056,-29.0729065858502));
#28124=CARTESIAN_POINT('Ctrl Pts',(-26.1016027155292,25.519195346557,-29.0730584759672));
#28125=CARTESIAN_POINT('Ctrl Pts',(-26.0968474818594,25.5253474855905,-29.0735398880642));
#28126=CARTESIAN_POINT('Ctrl Pts',(-26.0935805566796,25.529552528006,-29.0738688258547));
#28127=CARTESIAN_POINT('Ctrl Pts',(-26.0819098674858,25.544497921155,-29.0750376022537));
#28128=CARTESIAN_POINT('Ctrl Pts',(-26.0734482253182,25.5551931907378,-29.075873413166));
#28129=CARTESIAN_POINT('Ctrl Pts',(-25.8818857597726,25.7941889934861,-29.0945452236154));
#28130=CARTESIAN_POINT('Ctrl Pts',(-25.6685672168057,25.9965910085693,-29.1103398070627));
#28131=CARTESIAN_POINT('Ctrl Pts',(-25.3874961015267,26.1985536749705,-29.1298247459396));
#28132=CARTESIAN_POINT('Ctrl Pts',(-25.3434127134965,26.2285988847945,-29.132843821961));
#28133=CARTESIAN_POINT('Ctrl Pts',(-25.2093666288013,26.315165306086,-29.1419562739163));
#28134=CARTESIAN_POINT('Ctrl Pts',(-25.1173409524393,26.3683428325062,-29.1481261796362));
#28135=CARTESIAN_POINT('Ctrl Pts',(-24.9945922910384,26.431399944741,-29.1563520597774));
#28136=CARTESIAN_POINT('Ctrl Pts',(-24.9661084387559,26.4455037640826,-29.1582603601898));
#28137=CARTESIAN_POINT('Ctrl Pts',(-24.9254978612916,26.4648695470193,-29.1609824763531));
#28138=CARTESIAN_POINT('Ctrl Pts',(-24.9135396301744,26.4704820332343,-29.1617841962552));
#28139=CARTESIAN_POINT('Ctrl Pts',(-24.8924822323475,26.4802075994966,-29.1631963986441));
#28140=CARTESIAN_POINT('Ctrl Pts',(-24.8833977688225,26.4843522303837,-29.163805786847));
#28141=CARTESIAN_POINT('Ctrl Pts',(-24.8710533577024,26.4899149913908,-29.164634095819));
#28142=CARTESIAN_POINT('Ctrl Pts',(-24.8678100415018,26.4913700756089,-29.1648517446707));
#28143=CARTESIAN_POINT('Ctrl Pts',(-24.8617043644207,26.4940972056145,-29.1652615229575));
#28144=CARTESIAN_POINT('Ctrl Pts',(-24.858842541338,26.4953704512827,-29.1654536109171));
#28145=CARTESIAN_POINT('Ctrl Pts',(-24.8528765790236,26.4980143382492,-29.1658540922756));
#28146=CARTESIAN_POINT('Ctrl Pts',(-24.8497721235563,26.4993842525726,-29.1660625103156));
#28147=CARTESIAN_POINT('Ctrl Pts',(-24.8426086295729,26.5025318061895,-29.1665434884385));
#28148=CARTESIAN_POINT('Ctrl Pts',(-24.8385480835539,26.5043059789229,-29.166816166856));
#28149=CARTESIAN_POINT('Ctrl Pts',(-24.8258990503452,26.5098016753919,-29.1676657259697));
#28150=CARTESIAN_POINT('Ctrl Pts',(-24.8172980579573,26.5134941360726,-29.1682435987626));
#28151=CARTESIAN_POINT('Ctrl Pts',(-24.744167543798,26.5445129239736,-29.1731588563472));
#28152=CARTESIAN_POINT('Ctrl Pts',(-24.6787830639527,26.5697634102216,-29.1775663504581));
#28153=CARTESIAN_POINT('Ctrl Pts',(-24.6048937059054,26.5955631446181,-29.1825671672736));
#28154=CARTESIAN_POINT('Ctrl Pts',(-24.5971456932678,26.5982353797177,-29.1830917848841));
#28155=CARTESIAN_POINT('Ctrl Pts',(-24.5373087534623,26.6186176470773,-29.1871451528167));
#28156=CARTESIAN_POINT('Ctrl Pts',(-24.4847867009972,26.6350199136976,-29.1907138161595));
#28157=CARTESIAN_POINT('Ctrl Pts',(-24.2781412461083,26.693792047651,-29.2047915390161));
#28158=CARTESIAN_POINT('Ctrl Pts',(-24.1213830391341,26.7260144948076,-29.2155646733074));
#28159=CARTESIAN_POINT('Ctrl Pts',(-23.9441831418336,26.7488916604126,-29.2276587873675));
#28160=CARTESIAN_POINT('Ctrl Pts',(-23.925448596786,26.7511432694058,-29.228936183964));
#28161=CARTESIAN_POINT('Ctrl Pts',(-23.8849509625642,26.7556500416624,-29.2316937821234));
#28162=CARTESIAN_POINT('Ctrl Pts',(-23.8631824172781,26.7578483806063,-29.2331737678876));
#28163=CARTESIAN_POINT('Ctrl Pts',(-23.815533891302,26.7621705823165,-29.2364065824248));
#28164=CARTESIAN_POINT('Ctrl Pts',(-23.7896470491529,26.7642036905725,-29.2381586321875));
#28165=CARTESIAN_POINT('Ctrl Pts',(-23.7316354157073,26.7680550344347,-29.2420722144512));
#28166=CARTESIAN_POINT('Ctrl Pts',(-23.6995018850785,26.7697054976405,-29.2442313072394));
#28167=CARTESIAN_POINT('Ctrl Pts',(-23.54952267875,26.7751584691819,-29.2542546933018));
#28168=CARTESIAN_POINT('Ctrl Pts',(-23.4315345725427,26.772973742257,-29.2619875291052));
#28169=CARTESIAN_POINT('Ctrl Pts',(-23.3076494984088,26.7638643378415,-29.2697725269664));
#28170=CARTESIAN_POINT('Ctrl Pts',(-23.3013820339088,26.7633850451904,-29.2701654658527));
#28171=CARTESIAN_POINT('Ctrl Pts',(-23.2924727293388,26.7626774983935,-29.2707226998974));
#28172=CARTESIAN_POINT('Ctrl Pts',(-23.2898297581368,26.7624643199034,-29.2708878378797));
#28173=CARTESIAN_POINT('Ctrl Pts',(-23.2852804824809,26.7620917298774,-29.2711717942256));
#28174=CARTESIAN_POINT('Ctrl Pts',(-23.2833740543012,26.7619338826732,-29.2712907014308));
#28175=CARTESIAN_POINT('Ctrl Pts',(-23.2797184055553,26.761627927185,-29.2715185402341));
#28176=CARTESIAN_POINT('Ctrl Pts',(-23.2779691683028,26.7614800873536,-29.2716274870229));
#28177=CARTESIAN_POINT('Ctrl Pts',(-23.2738446755678,26.7611281043468,-29.2718841963246));
#28178=CARTESIAN_POINT('Ctrl Pts',(-23.2714695201314,26.7609227543324,-29.2720318902262));
#28179=CARTESIAN_POINT('Ctrl Pts',(-23.2644429821229,26.7603074015115,-29.2724684228279));
#28180=CARTESIAN_POINT('Ctrl Pts',(-23.2597922347245,26.7598899228019,-29.2727568410163));
#28181=CARTESIAN_POINT('Ctrl Pts',(-23.2188591733074,26.7561258304405,-29.2752909141835));
#28182=CARTESIAN_POINT('Ctrl Pts',(-23.1826332768724,26.7521740678932,-29.2775030777286));
#28183=CARTESIAN_POINT('Ctrl Pts',(-22.9025418799797,26.7168032448063,-29.2944242968928));
#28184=CARTESIAN_POINT('Ctrl Pts',(-22.662894899956,26.6581784939642,-29.3078710662029));
#28185=CARTESIAN_POINT('Ctrl Pts',(-22.3199191577746,26.5313152572039,-29.3283726114739));
#28186=CARTESIAN_POINT('Ctrl Pts',(-22.2100241677656,26.4835510573287,-29.3351413443454));
#28187=CARTESIAN_POINT('Ctrl Pts',(-22.0936865702591,26.4250817291775,-29.3426915969777));
#28188=CARTESIAN_POINT('Ctrl Pts',(-22.0843494206542,26.4203318622999,-29.3433003194745));
#28189=CARTESIAN_POINT('Ctrl Pts',(-22.0750360135777,26.4155367736458,-29.3439103255379));
#28190=CARTESIAN_POINT('',(-26.7730017063021,23.5525590581545,-29.1857734493121));
#28191=CARTESIAN_POINT('Ctrl Pts',(-22.0750360153461,26.4155367745563,-29.5927618641105));
#28192=CARTESIAN_POINT('Ctrl Pts',(-22.1637904272254,26.4612327555499,-29.5866100394058));
#28193=CARTESIAN_POINT('Ctrl Pts',(-22.2547296296025,26.5028317038812,-29.5804582147011));
#28194=CARTESIAN_POINT('Ctrl Pts',(-22.3474377521427,26.5401278081217,-29.5743063899964));
#28195=CARTESIAN_POINT('Ctrl Pts',(-22.4401181667825,26.5774127655855,-29.5681564039025));
#28196=CARTESIAN_POINT('Ctrl Pts',(-22.5345660482642,26.6103972724394,-29.5620064178085));
#28197=CARTESIAN_POINT('Ctrl Pts',(-22.6303447948988,26.6389233329101,-29.5558564317145));
#28198=CARTESIAN_POINT('Ctrl Pts',(-22.7261205394837,26.6674484992718,-29.5497066383832));
#28199=CARTESIAN_POINT('Ctrl Pts',(-22.8232266497658,26.6915153735237,-29.5435568450518));
#28200=CARTESIAN_POINT('Ctrl Pts',(-22.9212115556172,26.7110158909029,-29.5374070517205));
#28201=CARTESIAN_POINT('Ctrl Pts',(-23.0192196038505,26.7305210139753,-29.5312558059117));
#28202=CARTESIAN_POINT('Ctrl Pts',(-23.1181064339784,26.7454575528111,-29.5251045601029));
#28203=CARTESIAN_POINT('Ctrl Pts',(-23.2174114836804,26.7557687770527,-29.5189533142941));
#28204=CARTESIAN_POINT('Ctrl Pts',(-23.3168270587088,26.7660914775628,-29.5127952222227));
#28205=CARTESIAN_POINT('Ctrl Pts',(-23.4166613497563,26.7717785427884,-29.5066371301513));
#28206=CARTESIAN_POINT('Ctrl Pts',(-23.5164500562438,26.7728252547143,-29.5004790380799));
#28207=CARTESIAN_POINT('Ctrl Pts',(-23.6163016224669,26.7738726259938,-29.4943170668517));
#28208=CARTESIAN_POINT('Ctrl Pts',(-23.7161071133172,26.7702738400485,-29.4881550956234));
#28209=CARTESIAN_POINT('Ctrl Pts',(-23.8154056779686,26.7620762148251,-29.4819931243952));
#28210=CARTESIAN_POINT('Ctrl Pts',(-23.9148615618508,26.7538656020616,-29.475821390724));
#28211=CARTESIAN_POINT('Ctrl Pts',(-24.0138084862309,26.7410416609189,-29.4696496570529));
#28212=CARTESIAN_POINT('Ctrl Pts',(-24.1117942094486,26.7237030995532,-29.4634779233817));
#28213=CARTESIAN_POINT('Ctrl Pts',(-24.1572044138707,26.7156677696078,-29.4606177139711));
#28214=CARTESIAN_POINT('Ctrl Pts',(-24.2024083687602,26.706663527161,-29.4577575045606));
#28215=CARTESIAN_POINT('Ctrl Pts',(-24.2473622296468,26.6967038075795,-29.45489729515));
#28216=CARTESIAN_POINT('Ctrl Pts',(-24.3443688800026,26.6752115705164,-29.4487252038377));
#28217=CARTESIAN_POINT('Ctrl Pts',(-24.4405515237555,26.6491911330412,-29.4425531125254));
#28218=CARTESIAN_POINT('Ctrl Pts',(-24.53545518344,26.6187201129948,-29.436381021213));
#28219=CARTESIAN_POINT('Ctrl Pts',(-24.6302302580479,26.5882903781682,-29.4302172924743));
#28220=CARTESIAN_POINT('Ctrl Pts',(-24.7237293829445,26.5534221778618,-29.4240535637355));
#28221=CARTESIAN_POINT('Ctrl Pts',(-24.8155082173733,26.5142440317422,-29.4178898349967));
#28222=CARTESIAN_POINT('Ctrl Pts',(-24.9071898207412,26.4751073911913,-29.41173263615));
#28223=CARTESIAN_POINT('Ctrl Pts',(-24.9971543595918,26.431670052021,-29.4055754373033));
#28224=CARTESIAN_POINT('Ctrl Pts',(-25.0849740268791,26.3841098842646,-29.3994182384567));
#28225=CARTESIAN_POINT('Ctrl Pts',(-25.172729503315,26.3365844801069,-29.3932655401489));
#28226=CARTESIAN_POINT('Ctrl Pts',(-25.2583428443512,26.2849424450272,-29.3871128418412));
#28227=CARTESIAN_POINT('Ctrl Pts',(-25.3414084066746,26.2294087783553,-29.3809601435335));
#28228=CARTESIAN_POINT('Ctrl Pts',(-25.4244424704185,26.1738961701289,-29.3748097783378));
#28229=CARTESIAN_POINT('Ctrl Pts',(-25.5049303143946,26.1144951037006,-29.368659413142));
#28230=CARTESIAN_POINT('Ctrl Pts',(-25.5824937638322,26.0514748602564,-29.3625090479463));
#28231=CARTESIAN_POINT('Ctrl Pts',(-25.6600485516049,25.9884616544084,-29.3563593695741));
#28232=CARTESIAN_POINT('Ctrl Pts',(-25.7346792569647,25.9218303490014,-29.3502096912019));
#28233=CARTESIAN_POINT('Ctrl Pts',(-25.8060401997706,25.8518909826796,-29.3440600128297));
#28234=CARTESIAN_POINT('Ctrl Pts',(-25.8774122645609,25.7819407159336,-29.3379093759972));
#28235=CARTESIAN_POINT('Ctrl Pts',(-25.9455132443089,25.7086816682928,-29.3317587391648));
#28236=CARTESIAN_POINT('Ctrl Pts',(-26.0100345170859,25.6324605296719,-29.3256081023323));
#28237=CARTESIAN_POINT('Ctrl Pts',(-26.0746248140709,25.5561578504443,-29.3194508856105));
#28238=CARTESIAN_POINT('Ctrl Pts',(-26.1356274756683,25.476887084633,-29.3132936688887));
#28239=CARTESIAN_POINT('Ctrl Pts',(-26.1927744666104,25.3950276903482,-29.3071364521669));
#28240=CARTESIAN_POINT('Ctrl Pts',(-26.2499533396248,25.3131226270425,-29.300975800359));
#28241=CARTESIAN_POINT('Ctrl Pts',(-26.3032720263459,25.2286264265793,-29.2948151485512));
#28242=CARTESIAN_POINT('Ctrl Pts',(-26.3525072295006,25.1419453950072,-29.2886544967434));
#28243=CARTESIAN_POINT('Ctrl Pts',(-26.4018248206584,25.0551193152454,-29.2824835359744));
#28244=CARTESIAN_POINT('Ctrl Pts',(-26.4470450824199,24.9661014890839,-29.2763125752054));
#28245=CARTESIAN_POINT('Ctrl Pts',(-26.4879917950637,24.8753206744542,-29.2701416144363));
#28246=CARTESIAN_POINT('Ctrl Pts',(-26.519247189636,24.8060259741559,-29.265431204216));
#28247=CARTESIAN_POINT('Ctrl Pts',(-26.5480135503193,24.7357045242288,-29.2607207939956));
#28248=CARTESIAN_POINT('Ctrl Pts',(-26.5742321263537,24.6645527486836,-29.2560103837753));
#28249=CARTESIAN_POINT('Ctrl Pts',(-26.6138607220893,24.5570089619713,-29.2488907392101));
#28250=CARTESIAN_POINT('Ctrl Pts',(-26.647783099162,24.447255320658,-29.2417710946449));
#28251=CARTESIAN_POINT('Ctrl Pts',(-26.6757817560599,24.3358635233027,-29.2346514500797));
#28252=CARTESIAN_POINT('Ctrl Pts',(-26.7036600285425,24.2249506716497,-29.2275624174918));
#28253=CARTESIAN_POINT('Ctrl Pts',(-26.7256653011929,24.1124138660151,-29.2204733849039));
#28254=CARTESIAN_POINT('Ctrl Pts',(-26.7416295934255,23.9988392149064,-29.2133843523159));
#28255=CARTESIAN_POINT('Ctrl Pts',(-26.7574726370541,23.8861271618817,-29.2063491608437));
#28256=CARTESIAN_POINT('Ctrl Pts',(-26.7673660173076,23.7723931300587,-29.1993139693714));
#28257=CARTESIAN_POINT('Ctrl Pts',(-26.7711931727418,23.6582291465142,-29.1922787778991));
#28258=CARTESIAN_POINT('Ctrl Pts',(-26.7723728091336,23.6230406123812,-29.1901103350368));
#28259=CARTESIAN_POINT('Ctrl Pts',(-26.7729764761766,23.5878113596244,-29.1879418921745));
#28260=CARTESIAN_POINT('Ctrl Pts',(-26.7730017063021,23.5525590581545,-29.1857734493121));
#28261=CARTESIAN_POINT('Ctrl Pts',(-26.7730017875139,23.5524426489476,-29.1878050506611));
#28262=CARTESIAN_POINT('Ctrl Pts',(-26.7730978322047,23.4111132496054,-29.1797069801023));
#28263=CARTESIAN_POINT('Ctrl Pts',(-26.7638973695217,23.2699447972146,-29.1714120560357));
#28264=CARTESIAN_POINT('Ctrl Pts',(-26.744572087701,23.1230677348811,-29.1623918435185));
#28265=CARTESIAN_POINT('Ctrl Pts',(-26.7436589419758,23.1162942685426,-29.1619750092687));
#28266=CARTESIAN_POINT('Ctrl Pts',(-26.7421316500873,23.1052311455476,-29.1612927794928));
#28267=CARTESIAN_POINT('Ctrl Pts',(-26.7415303834496,23.1009397084099,-29.1610277915846));
#28268=CARTESIAN_POINT('Ctrl Pts',(-26.7404540131282,23.0933684618979,-29.1605596629691));
#28269=CARTESIAN_POINT('Ctrl Pts',(-26.7399825013429,23.0900881415331,-29.1603566362779));
#28270=CARTESIAN_POINT('Ctrl Pts',(-26.7390458587803,23.0836425069241,-29.1599572952329));
#28271=CARTESIAN_POINT('Ctrl Pts',(-26.7385810726079,23.0804771458343,-29.1597609920217));
#28272=CARTESIAN_POINT('Ctrl Pts',(-26.7376474138155,23.0741838055142,-29.1593703190914));
#28273=CARTESIAN_POINT('Ctrl Pts',(-26.7371786481747,23.0710558136392,-29.1591759529613));
#28274=CARTESIAN_POINT('Ctrl Pts',(-26.7360595035004,23.0636622325974,-29.1587160834287));
#28275=CARTESIAN_POINT('Ctrl Pts',(-26.735405162214,23.0593972568973,-29.1584504543809));
#28276=CARTESIAN_POINT('Ctrl Pts',(-26.7334352255732,23.0467270823126,-29.1576602775376));
#28277=CARTESIAN_POINT('Ctrl Pts',(-26.7320949185329,23.0383258144043,-29.1571349449975));
#28278=CARTESIAN_POINT('Ctrl Pts',(-26.7195282007226,22.9615118130368,-29.1523189045252));
#28279=CARTESIAN_POINT('Ctrl Pts',(-26.7061310172942,22.8934773202314,-29.147959382976));
#28280=CARTESIAN_POINT('Ctrl Pts',(-26.6774694265848,22.7692147556738,-29.1398137491908));
#28281=CARTESIAN_POINT('Ctrl Pts',(-26.6628540108267,22.7128655940036,-29.1360493975091));
#28282=CARTESIAN_POINT('Ctrl Pts',(-26.6414100372519,22.6385343577541,-29.1309907238798));
#28283=CARTESIAN_POINT('Ctrl Pts',(-26.6359344826545,22.6201710142091,-29.1297333745749));
#28284=CARTESIAN_POINT('Ctrl Pts',(-26.5623348694739,22.3811460790395,-29.1132691276442));
#28285=CARTESIAN_POINT('Ctrl Pts',(-26.4708490317124,22.1683884474793,-29.0974506762419));
#28286=CARTESIAN_POINT('Ctrl Pts',(-26.2920295268063,21.8512804912174,-29.0730389994483));
#28287=CARTESIAN_POINT('Ctrl Pts',(-26.219491580603,21.7394461910802,-29.0642607777098));
#28288=CARTESIAN_POINT('Ctrl Pts',(-26.1367677658436,21.627730648971,-29.0555536027452));
#28289=CARTESIAN_POINT('Ctrl Pts',(-26.1332910408018,21.6230619578884,-29.0551898483074));
#28290=CARTESIAN_POINT('Ctrl Pts',(-26.1282612931955,21.6163458660896,-29.0546667867535));
#28291=CARTESIAN_POINT('Ctrl Pts',(-26.1267184672577,21.6142908976119,-29.0545067709204));
#28292=CARTESIAN_POINT('Ctrl Pts',(-26.1240314701585,21.6107208503455,-29.0542288327711));
#28293=CARTESIAN_POINT('Ctrl Pts',(-26.1228884166142,21.6092049354887,-29.0541108314192));
#28294=CARTESIAN_POINT('Ctrl Pts',(-26.1206737563305,21.6062732511622,-29.053882658039));
#28295=CARTESIAN_POINT('Ctrl Pts',(-26.1196023218151,21.6048573607219,-29.0537724742252));
#28296=CARTESIAN_POINT('Ctrl Pts',(-26.1170430173746,21.6014810668913,-29.0535097670928));
#28297=CARTESIAN_POINT('Ctrl Pts',(-26.1155540682241,21.5995214774018,-29.053357320312));
#28298=CARTESIAN_POINT('Ctrl Pts',(-26.1110494180498,21.5936070337708,-29.0528972814162));
#28299=CARTESIAN_POINT('Ctrl Pts',(-26.1080267874823,21.5896574294555,-29.0525901761172));
#28300=CARTESIAN_POINT('Ctrl Pts',(-26.0772325074866,21.5496116446586,-29.0494772548016));
#28301=CARTESIAN_POINT('Ctrl Pts',(-26.0487060704095,21.5140987572732,-29.0467239433665));
#28302=CARTESIAN_POINT('Ctrl Pts',(-26.0175118019993,21.4769078405047,-29.0438339126906));
#28303=CARTESIAN_POINT('Ctrl Pts',(-26.015585750564,21.4746180177553,-29.04365594797));
#28304=CARTESIAN_POINT('Ctrl Pts',(-26.0117202351808,21.4700353974643,-29.0432997250141));
#28305=CARTESIAN_POINT('Ctrl Pts',(-26.0097807499415,21.4677426218444,-29.0431214682556));
#28306=CARTESIAN_POINT('Ctrl Pts',(-26.0047167776538,21.4617731546945,-29.0426572673003));
#28307=CARTESIAN_POINT('Ctrl Pts',(-26.0015872231578,21.4581007509231,-29.0423716006928));
#28308=CARTESIAN_POINT('Ctrl Pts',(-25.9950613792114,21.4504776857515,-29.0417783993475));
#28309=CARTESIAN_POINT('Ctrl Pts',(-25.9916637312353,21.4465282009115,-29.041470938331));
#28310=CARTESIAN_POINT('Ctrl Pts',(-25.8155682578971,21.2428329530368,-29.0256060609946));
#28311=CARTESIAN_POINT('Ctrl Pts',(-25.6189684505117,21.0650389092865,-29.011311710947));
#28312=CARTESIAN_POINT('Ctrl Pts',(-25.3508928804503,20.8767071381769,-28.9927839516359));
#28313=CARTESIAN_POINT('Ctrl Pts',(-25.2978622993952,20.8417455230738,-28.9891641270716));
#28314=CARTESIAN_POINT('Ctrl Pts',(-25.1737167013367,20.7650642010329,-28.9807431975298));
#28315=CARTESIAN_POINT('Ctrl Pts',(-25.1019673969194,20.7244624990995,-28.9759140970834));
#28316=CARTESIAN_POINT('Ctrl Pts',(-24.9908675854954,20.667100962717,-28.9684399780985));
#28317=CARTESIAN_POINT('Ctrl Pts',(-24.9526074542006,20.6482988606401,-28.9658668952078));
#28318=CARTESIAN_POINT('Ctrl Pts',(-24.9071202726928,20.6270548078539,-28.9628048494863));
#28319=CARTESIAN_POINT('Ctrl Pts',(-24.9002423026352,20.6238720683855,-28.9623417722362));
#28320=CARTESIAN_POINT('Ctrl Pts',(-24.8903390209827,20.6193317277861,-28.9616748783384));
#28321=CARTESIAN_POINT('Ctrl Pts',(-24.8873227039497,20.617954471829,-28.9614717402185));
#28322=CARTESIAN_POINT('Ctrl Pts',(-24.8813931506945,20.6152580782002,-28.961072369919));
#28323=CARTESIAN_POINT('Ctrl Pts',(-24.8784800653019,20.613938616521,-28.9608761491836));
#28324=CARTESIAN_POINT('Ctrl Pts',(-24.8726837850013,20.6113236223774,-28.9604856849874));
#28325=CARTESIAN_POINT('Ctrl Pts',(-24.8698006381139,20.6100279912099,-28.9602914451794));
#28326=CARTESIAN_POINT('Ctrl Pts',(-24.8629844746599,20.6069769825097,-28.9598321908792));
#28327=CARTESIAN_POINT('Ctrl Pts',(-24.8590498428713,20.6052252465089,-28.9595670515512));
#28328=CARTESIAN_POINT('Ctrl Pts',(-24.845334809303,20.599152094943,-28.9586427205044));
#28329=CARTESIAN_POINT('Ctrl Pts',(-24.8355365031388,20.5948715068701,-28.9579821307434));
#28330=CARTESIAN_POINT('Ctrl Pts',(-24.714536864437,20.5427259140448,-28.949821262496));
#28331=CARTESIAN_POINT('Ctrl Pts',(-24.6007588445094,20.5011207606099,-28.9421083247538));
#28332=CARTESIAN_POINT('Ctrl Pts',(-24.3327012309122,20.4198866280059,-28.9238223284591));
#28333=CARTESIAN_POINT('Ctrl Pts',(-24.1772886262071,20.3850932526665,-28.9131300683707));
#28334=CARTESIAN_POINT('Ctrl Pts',(-24.0019307036954,20.3592595124698,-28.901136047765));
#28335=CARTESIAN_POINT('Ctrl Pts',(-23.9838806593071,20.3567566000239,-28.8999025020582));
#28336=CARTESIAN_POINT('Ctrl Pts',(-23.9450401234547,20.3517061403668,-28.8972511733862));
#28337=CARTESIAN_POINT('Ctrl Pts',(-23.9242439999695,20.3492079139723,-28.8958334595716));
#28338=CARTESIAN_POINT('Ctrl Pts',(-23.8790394740103,20.3442240555681,-28.892757217207));
#28339=CARTESIAN_POINT('Ctrl Pts',(-23.8546239296,20.3418140471437,-28.8910991318945));
#28340=CARTESIAN_POINT('Ctrl Pts',(-23.748166612865,20.3325319994976,-28.8838893005205));
#28341=CARTESIAN_POINT('Ctrl Pts',(-23.6659019234487,20.3285259790501,-28.8783682569127));
#28342=CARTESIAN_POINT('Ctrl Pts',(-23.5087905137374,20.3269016204149,-28.8680139259658));
#28343=CARTESIAN_POINT('Ctrl Pts',(-23.433999207243,20.328731553804,-28.8631671609071));
#28344=CARTESIAN_POINT('Ctrl Pts',(-23.3477463155057,20.3338502686176,-28.8577226574796));
#28345=CARTESIAN_POINT('Ctrl Pts',(-23.3361632639188,20.3346004857259,-28.8569945425464));
#28346=CARTESIAN_POINT('Ctrl Pts',(-23.3212266133829,20.335648975901,-28.8560597580245));
#28347=CARTESIAN_POINT('Ctrl Pts',(-23.3178692701128,20.3358899335792,-28.8558499143927));
#28348=CARTESIAN_POINT('Ctrl Pts',(-23.3124524438862,20.336287232171,-28.855511789468));
#28349=CARTESIAN_POINT('Ctrl Pts',(-23.3103927342609,20.3364402929451,-28.855383323093));
#28350=CARTESIAN_POINT('Ctrl Pts',(-23.3064563567602,20.3367366176271,-28.8551380060102));
#28351=CARTESIAN_POINT('Ctrl Pts',(-23.3045796810269,20.3368795444213,-28.8550211373786));
#28352=CARTESIAN_POINT('Ctrl Pts',(-23.3002884806279,20.3372101415671,-28.8547541028295));
#28353=CARTESIAN_POINT('Ctrl Pts',(-23.2978740442107,20.3373988894118,-28.8546039987214));
#28354=CARTESIAN_POINT('Ctrl Pts',(-23.2914856275526,20.3379055477404,-28.85420720605));
#28355=CARTESIAN_POINT('Ctrl Pts',(-23.2875120046881,20.338228112131,-28.8539607797343));
#28356=CARTESIAN_POINT('Ctrl Pts',(-23.2616566056573,20.340375260849,-28.8523597604061));
#28357=CARTESIAN_POINT('Ctrl Pts',(-23.2397926723898,20.3424161204473,-28.8510171683383));
#28358=CARTESIAN_POINT('Ctrl Pts',(-23.212129218147,20.3452838204643,-28.8493307999366));
#28359=CARTESIAN_POINT('Ctrl Pts',(-23.2063094478701,20.345903148232,-28.848976719384));
#28360=CARTESIAN_POINT('Ctrl Pts',(-23.1972182861481,20.3468956635614,-28.8484246431366));
#28361=CARTESIAN_POINT('Ctrl Pts',(-23.19394575607,20.3472580132822,-28.8482261236804));
#28362=CARTESIAN_POINT('Ctrl Pts',(-22.9372563832404,20.3760781168246,-28.8326708500973));
#28363=CARTESIAN_POINT('Ctrl Pts',(-22.688072301185,20.4345129588063,-28.8187512422246));
#28364=CARTESIAN_POINT('Ctrl Pts',(-22.3377715968158,20.5619661320368,-28.7978450164624));
#28365=CARTESIAN_POINT('Ctrl Pts',(-22.2294787618548,20.6082261051504,-28.7911886111177));
#28366=CARTESIAN_POINT('Ctrl Pts',(-22.0572184094176,20.6932424326598,-28.780047070728));
#28367=CARTESIAN_POINT('Ctrl Pts',(-21.9916385807724,20.7284837749121,-28.7756673038632));
#28368=CARTESIAN_POINT('Ctrl Pts',(-21.9057698650325,20.7785350649673,-28.7697122790831));
#28369=CARTESIAN_POINT('Ctrl Pts',(-21.8843462381465,20.7913583466394,-28.768207687774));
#28370=CARTESIAN_POINT('Ctrl Pts',(-21.8536701141095,20.8102073697275,-28.7660249302696));
#28371=CARTESIAN_POINT('Ctrl Pts',(-21.8442958509804,20.8160339617762,-28.7653540360045));
#28372=CARTESIAN_POINT('Ctrl Pts',(-21.8276914572692,20.8264730885345,-28.7641587096565));
#28373=CARTESIAN_POINT('Ctrl Pts',(-21.8204494252323,20.8310665651339,-28.7636349843473));
#28374=CARTESIAN_POINT('Ctrl Pts',(-21.8096553014972,20.8379736349204,-28.7628507796498));
#28375=CARTESIAN_POINT('Ctrl Pts',(-21.8060892591045,20.8402654450218,-28.7625911125401));
#28376=CARTESIAN_POINT('Ctrl Pts',(-21.7998068596887,20.8443205296667,-28.7621326025134));
#28377=CARTESIAN_POINT('Ctrl Pts',(-21.7970886138773,20.8460808789732,-28.7619338691828));
#28378=CARTESIAN_POINT('Ctrl Pts',(-21.791672304423,20.8496001068204,-28.7615371833804));
#28379=CARTESIAN_POINT('Ctrl Pts',(-21.7889742146708,20.851358938834,-28.7613392327984));
#28380=CARTESIAN_POINT('Ctrl Pts',(-21.7824847433342,20.8556031740254,-28.7608622866739));
#28381=CARTESIAN_POINT('Ctrl Pts',(-21.7786959680197,20.8580925335286,-28.7605831426332));
#28382=CARTESIAN_POINT('Ctrl Pts',(-21.767083188397,20.8657576705535,-28.7597254339427));
#28383=CARTESIAN_POINT('Ctrl Pts',(-21.7592765729207,20.870959587936,-28.7591458847152));
#28384=CARTESIAN_POINT('Ctrl Pts',(-21.668391809895,20.9320951000328,-28.7523638350446));
#28385=CARTESIAN_POINT('Ctrl Pts',(-21.5879501309053,20.9918323543447,-28.7460164624855));
#28386=CARTESIAN_POINT('Ctrl Pts',(-21.3073057961999,21.2212738091584,-28.7225475816191));
#28387=CARTESIAN_POINT('Ctrl Pts',(-21.1252441958995,21.4115033235543,-28.7046161273414));
#28388=CARTESIAN_POINT('Ctrl Pts',(-20.9468391219765,21.6503473015461,-28.6845635052697));
#28389=CARTESIAN_POINT('Ctrl Pts',(-20.9258775914347,21.679408458616,-28.6821622980976));
#28390=CARTESIAN_POINT('Ctrl Pts',(-20.8759840157796,21.7510703115994,-28.6763440716493));
#28391=CARTESIAN_POINT('Ctrl Pts',(-20.8475789100175,21.794028015299,-28.6729424642591));
#28392=CARTESIAN_POINT('Ctrl Pts',(-20.7981253501123,21.8728613128955,-28.6668769919587));
#28393=CARTESIAN_POINT('Ctrl Pts',(-20.7767186442866,21.9084987533439,-28.6641978893532));
#28394=CARTESIAN_POINT('Ctrl Pts',(-20.7456497249463,21.9625646759178,-28.6602378257455));
#28395=CARTESIAN_POINT('Ctrl Pts',(-20.735467407305,21.9806874998422,-28.6589276349974));
#28396=CARTESIAN_POINT('Ctrl Pts',(-20.7234969515208,22.0024841068837,-28.6573734971663));
#28397=CARTESIAN_POINT('Ctrl Pts',(-20.7215398484717,22.0060638246068,-28.6571189501576));
#28398=CARTESIAN_POINT('Ctrl Pts',(-20.7185265993363,22.0116002803441,-28.6567263448873));
#28399=CARTESIAN_POINT('Ctrl Pts',(-20.7174656808087,22.0135543947478,-28.6565879810183));
#28400=CARTESIAN_POINT('Ctrl Pts',(-20.7156071445307,22.016986112899,-28.6563453598468));
#28401=CARTESIAN_POINT('Ctrl Pts',(-20.714808662411,22.0184632360818,-28.6562410469593));
#28402=CARTESIAN_POINT('Ctrl Pts',(-20.7131188323505,22.0215951249323,-28.6560201287088));
#28403=CARTESIAN_POINT('Ctrl Pts',(-20.7122277801546,22.0232500415547,-28.6559035426119));
#28404=CARTESIAN_POINT('Ctrl Pts',(-20.7096972042968,22.0279598479969,-28.6555721655314));
#28405=CARTESIAN_POINT('Ctrl Pts',(-20.7080611554445,22.0310166172015,-28.6553575976185));
#28406=CARTESIAN_POINT('Ctrl Pts',(-20.7011449269301,22.0439890688454,-28.6544491112207));
#28407=CARTESIAN_POINT('Ctrl Pts',(-20.6959115969542,22.0539298391925,-28.6537581502749));
#28408=CARTESIAN_POINT('Ctrl Pts',(-20.6050295978417,22.228773111704,-28.6416927508709));
#28409=CARTESIAN_POINT('Ctrl Pts',(-20.5337346761073,22.400779568126,-28.6311755735118));
#28410=CARTESIAN_POINT('Ctrl Pts',(-20.389182143201,22.8576051345413,-28.6043264995181));
#28411=CARTESIAN_POINT('Ctrl Pts',(-20.3392943206521,23.147941418624,-28.5881471858314));
#28412=CARTESIAN_POINT('Ctrl Pts',(-20.3287100462353,23.4600136944735,-28.5693493968427));
#28413=CARTESIAN_POINT('Ctrl Pts',(-20.3282337608482,23.4790201658713,-28.5681997495099));
#28414=CARTESIAN_POINT('Ctrl Pts',(-20.3277795947686,23.5070436185374,-28.5664972167989));
#28415=CARTESIAN_POINT('Ctrl Pts',(-20.3276713315218,23.516058305461,-28.5659484005843));
#28416=CARTESIAN_POINT('Ctrl Pts',(-20.3275441137625,23.5323406855082,-28.5649550188217));
#28417=CARTESIAN_POINT('Ctrl Pts',(-20.3275119155594,23.5396082378426,-28.5645108702719));
#28418=CARTESIAN_POINT('Ctrl Pts',(-20.3275001498358,23.5508373964193,-28.5638234208343));
#28419=CARTESIAN_POINT('Ctrl Pts',(-20.3275033037355,23.5547989927359,-28.5635806626337));
#28420=CARTESIAN_POINT('Ctrl Pts',(-20.3275217297088,23.5617785305081,-28.5631525640811));
#28421=CARTESIAN_POINT('Ctrl Pts',(-20.3275339364467,23.564796481065,-28.5629673201907));
#28422=CARTESIAN_POINT('Ctrl Pts',(-20.3275709938322,23.5715967200886,-28.5625496125246));
#28423=CARTESIAN_POINT('Ctrl Pts',(-20.3275982638655,23.5753789859878,-28.5623170730586));
#28424=CARTESIAN_POINT('Ctrl Pts',(-20.3276892751585,23.5855245596403,-28.5616927342797));
#28425=CARTESIAN_POINT('Ctrl Pts',(-20.3277652053051,23.5918877170724,-28.5613005528182));
#28426=CARTESIAN_POINT('Ctrl Pts',(-20.3281774760633,23.6195658935915,-28.5595919943545));
#28427=CARTESIAN_POINT('Ctrl Pts',(-20.3287064500831,23.6408771152084,-28.5582695834757));
#28428=CARTESIAN_POINT('Ctrl Pts',(-20.3299018714579,23.6752760136589,-28.5561235542816));
#28429=CARTESIAN_POINT('Ctrl Pts',(-20.3304367923625,23.68836785485,-28.5553041093124));
#28430=CARTESIAN_POINT('Ctrl Pts',(-20.3313207361289,23.707187490914,-28.554122219375));
#28431=CARTESIAN_POINT('Ctrl Pts',(-20.3316052489282,23.7129183067775,-28.5537617947625));
#28432=CARTESIAN_POINT('Ctrl Pts',(-20.3323601474497,23.7273457816071,-28.5528530887614));
#28433=CARTESIAN_POINT('Ctrl Pts',(-20.3328504829972,23.7360413106617,-28.5523041906726));
#28434=CARTESIAN_POINT('Ctrl Pts',(-20.3334693737092,23.7462782142428,-28.5516565524522));
#28435=CARTESIAN_POINT('Ctrl Pts',(-20.3335638018583,23.7478216817356,-28.55155886629));
#28436=CARTESIAN_POINT('Ctrl Pts',(-20.3532645815474,24.0660808513355,-28.5314082498986));
#28437=CARTESIAN_POINT('Ctrl Pts',(-20.4195393688342,24.3781153774592,-28.5097640448727));
#28438=CARTESIAN_POINT('Ctrl Pts',(-20.5820092018874,24.8142198702219,-28.478450090031));
#28439=CARTESIAN_POINT('Ctrl Pts',(-20.6432743851476,24.9493851986291,-28.4686253341562));
#28440=CARTESIAN_POINT('Ctrl Pts',(-20.7165361692649,25.08524649767,-28.4589536416341));
#28441=CARTESIAN_POINT('Ctrl Pts',(-20.7194516232791,25.0906164876008,-28.4585717185055));
#28442=CARTESIAN_POINT('Ctrl Pts',(-20.7236395539426,25.0982782120599,-28.458027347838));
#28443=CARTESIAN_POINT('Ctrl Pts',(-20.7248995581056,25.1005766938669,-28.457864109409));
#28444=CARTESIAN_POINT('Ctrl Pts',(-20.7270813490224,25.1045451921739,-28.4575823910894));
#28445=CARTESIAN_POINT('Ctrl Pts',(-20.728001815516,25.1062159297837,-28.4574638260143));
#28446=CARTESIAN_POINT('Ctrl Pts',(-20.7297756467799,25.1094288561361,-28.4572358935095));
#28447=CARTESIAN_POINT('Ctrl Pts',(-20.7306287916589,25.1109711590266,-28.4571265121238));
#28448=CARTESIAN_POINT('Ctrl Pts',(-20.7326520855379,25.1146217663981,-28.456867684811));
#28449=CARTESIAN_POINT('Ctrl Pts',(-20.7338233382753,25.1167294626494,-28.45671831027));
#28450=CARTESIAN_POINT('Ctrl Pts',(-20.737321466759,25.1230078194232,-28.4562735318395));
#28451=CARTESIAN_POINT('Ctrl Pts',(-20.7396552621872,25.1271746478721,-28.4559785711346));
#28452=CARTESIAN_POINT('Ctrl Pts',(-20.7613322996444,25.1656764860252,-28.4532550994881));
#28453=CARTESIAN_POINT('Ctrl Pts',(-20.7812956043339,25.1996610595797,-28.4508658195019));
#28454=CARTESIAN_POINT('Ctrl Pts',(-20.803234317856,25.2354870070532,-28.4483534852167));
#28455=CARTESIAN_POINT('Ctrl Pts',(-20.8045929490365,25.2376996450414,-28.4481983479061));
#28456=CARTESIAN_POINT('Ctrl Pts',(-20.8066545361579,25.2410480206287,-28.4479636154648));
#28457=CARTESIAN_POINT('Ctrl Pts',(-20.8073555233706,25.242184961862,-28.4478839183709));
#28458=CARTESIAN_POINT('Ctrl Pts',(-20.809763756394,25.2460854795346,-28.4476105211679));
#28459=CARTESIAN_POINT('Ctrl Pts',(-20.8114744791637,25.2488469193212,-28.4474170002688));
#28460=CARTESIAN_POINT('Ctrl Pts',(-20.8181204991471,25.259538747383,-28.4466678385315));
#28461=CARTESIAN_POINT('Ctrl Pts',(-20.8230861360351,25.2674503259406,-28.4461137380288));
#28462=CARTESIAN_POINT('Ctrl Pts',(-20.9067392098813,25.3994538047281,-28.4368709550051));
#28463=CARTESIAN_POINT('Ctrl Pts',(-20.9937964206793,25.5180555047688,-28.4285955642676));
#28464=CARTESIAN_POINT('Ctrl Pts',(-21.2232943471133,25.7896499278746,-28.4086932174755));
#28465=CARTESIAN_POINT('Ctrl Pts',(-21.3730785653031,25.9355285963084,-28.3971377995706));
#28466=CARTESIAN_POINT('Ctrl Pts',(-21.6062643214353,26.1222463147299,-28.3797478217694));
#28467=CARTESIAN_POINT('Ctrl Pts',(-21.6789512606303,26.1756042134507,-28.3744052371149));
#28468=CARTESIAN_POINT('Ctrl Pts',(-21.7629865289072,26.2320282364482,-28.3682690981738));
#28469=CARTESIAN_POINT('Ctrl Pts',(-21.7722308742147,26.2381661605273,-28.3675946460266));
#28470=CARTESIAN_POINT('Ctrl Pts',(-21.7887106377258,26.2489859358252,-28.3663932032738));
#28471=CARTESIAN_POINT('Ctrl Pts',(-21.7959335169198,26.2536867592846,-28.3658669280088));
#28472=CARTESIAN_POINT('Ctrl Pts',(-21.8067422644647,26.2606597946396,-28.3650797949164));
#28473=CARTESIAN_POINT('Ctrl Pts',(-21.8103139494466,26.2629540104226,-28.3648197591482));
#28474=CARTESIAN_POINT('Ctrl Pts',(-21.8166167627524,26.2669849547422,-28.3643609986512));
#28475=CARTESIAN_POINT('Ctrl Pts',(-21.8193459995205,26.268724642007,-28.3641623844399));
#28476=CARTESIAN_POINT('Ctrl Pts',(-21.8247940363646,26.272185833388,-28.3637659885104));
#28477=CARTESIAN_POINT('Ctrl Pts',(-21.8275128036597,26.2739073826803,-28.3635682087591));
#28478=CARTESIAN_POINT('Ctrl Pts',(-21.8340592725838,26.2780389455092,-28.3630920629843));
#28479=CARTESIAN_POINT('Ctrl Pts',(-21.8378894710184,26.2804449736511,-28.3628135495515));
#28480=CARTESIAN_POINT('Ctrl Pts',(-21.8496437075298,26.2877942054343,-28.3619590420407));
#28481=CARTESIAN_POINT('Ctrl Pts',(-21.8575841259507,26.2927110005755,-28.3613820733927));
#28482=CARTESIAN_POINT('Ctrl Pts',(-21.9338952363816,26.339506015508,-28.3558396228713));
#28483=CARTESIAN_POINT('Ctrl Pts',(-22.0037740529195,26.3788469336282,-28.3507823253816));
#28484=CARTESIAN_POINT('Ctrl Pts',(-22.0750360250495,26.4155367795522,-28.3456357132216));
#28485=CARTESIAN_POINT('Origin',(-23.5502525316942,23.5502525316942,-77.3107734492734));
#28486=CARTESIAN_POINT('',(-22.0750359193537,26.4155367251338,-26.8471666088699));
#28487=CARTESIAN_POINT('',(-22.075036065511,26.4155368003841,-27.0910469152906));
#28488=CARTESIAN_POINT('',(-22.0750360153461,26.4155367745563,-77.3107734492734));
#28489=CARTESIAN_POINT('Ctrl Pts',(-22.0750359193537,26.4155367251338,-26.8471666088699));
#28490=CARTESIAN_POINT('Ctrl Pts',(-22.0260367658724,26.390309082664,-26.8508920404459));
#28491=CARTESIAN_POINT('Ctrl Pts',(-21.9776797507882,26.3638219780101,-26.8546086240552));
#28492=CARTESIAN_POINT('Ctrl Pts',(-21.8781595643101,26.3059413752287,-26.8623136408831));
#28493=CARTESIAN_POINT('Ctrl Pts',(-21.8271551177872,26.2743398862597,-26.8662947903275));
#28494=CARTESIAN_POINT('Ctrl Pts',(-21.738688681582,26.2160480245785,-26.8732220726755));
#28495=CARTESIAN_POINT('Ctrl Pts',(-21.7008600709887,26.189945166315,-26.8761915947194));
#28496=CARTESIAN_POINT('Ctrl Pts',(-21.6516467702822,26.1544090410951,-26.8800514157724));
#28497=CARTESIAN_POINT('Ctrl Pts',(-21.6397520395683,26.1456952398626,-26.8809840513181));
#28498=CARTESIAN_POINT('Ctrl Pts',(-21.620268116247,26.1312152481546,-26.8825107149833));
#28499=CARTESIAN_POINT('Ctrl Pts',(-21.612644096435,26.1254965870606,-26.8831078348526));
#28500=CARTESIAN_POINT('Ctrl Pts',(-21.6031705806084,26.118324759632,-26.8838493652823));
#28501=CARTESIAN_POINT('Ctrl Pts',(-21.6012972651902,26.1169033574592,-26.8839959755264));
#28502=CARTESIAN_POINT('Ctrl Pts',(-21.5976569202388,26.1141349154017,-26.88428083274));
#28503=CARTESIAN_POINT('Ctrl Pts',(-21.5958897253786,26.1127880964664,-26.8844190951337));
#28504=CARTESIAN_POINT('Ctrl Pts',(-21.5927896310873,26.1104203726923,-26.8846616028622));
#28505=CARTESIAN_POINT('Ctrl Pts',(-21.5914561420157,26.1094002580186,-26.8847659036036));
#28506=CARTESIAN_POINT('Ctrl Pts',(-21.5886308242752,26.1072353973833,-26.8849868629702));
#28507=CARTESIAN_POINT('Ctrl Pts',(-21.5871392046254,26.1060903911004,-26.8851035022259));
#28508=CARTESIAN_POINT('Ctrl Pts',(-21.5828965887288,26.1028277428331,-26.8854352174195));
#28509=CARTESIAN_POINT('Ctrl Pts',(-21.5801480001898,26.1007069520001,-26.8856500695361));
#28510=CARTESIAN_POINT('Ctrl Pts',(-21.5684890295062,26.09168088228,-26.8865612413888));
#28511=CARTESIAN_POINT('Ctrl Pts',(-21.5596113436682,26.0847332100937,-26.8872545818093));
#28512=CARTESIAN_POINT('Ctrl Pts',(-21.41087107141,25.9670654949637,-26.8988666419973));
#28513=CARTESIAN_POINT('Ctrl Pts',(-21.2803791194128,25.8449491498019,-26.9089956370651));
#28514=CARTESIAN_POINT('Ctrl Pts',(-21.0456744101102,25.5855828122911,-26.928618496798));
#28515=CARTESIAN_POINT('Ctrl Pts',(-20.9410178326508,25.4495612646637,-26.9380960457788));
#28516=CARTESIAN_POINT('Ctrl Pts',(-20.8092052211597,25.2466497277178,-26.9519072738813));
#28517=CARTESIAN_POINT('Ctrl Pts',(-20.7726966531897,25.1861884320487,-26.955982907929));
#28518=CARTESIAN_POINT('Ctrl Pts',(-20.7002369447813,25.0567615842695,-26.9646796958136));
#28519=CARTESIAN_POINT('Ctrl Pts',(-20.6647375153548,24.9875972882442,-26.9693116594756));
#28520=CARTESIAN_POINT('Ctrl Pts',(-20.62625933619,24.9054464025964,-26.974823299408));
#28521=CARTESIAN_POINT('Ctrl Pts',(-20.6208154210256,24.8936381211498,-26.9756157458324));
#28522=CARTESIAN_POINT('Ctrl Pts',(-20.6133390157772,24.8771596491318,-26.9767220076204));
#28523=CARTESIAN_POINT('Ctrl Pts',(-20.6112458609511,24.8725169860069,-26.977033731123));
#28524=CARTESIAN_POINT('Ctrl Pts',(-20.6077316579981,24.8646728370825,-26.9775604945887));
#28525=CARTESIAN_POINT('Ctrl Pts',(-20.6063048038795,24.861473949722,-26.9777753345429));
#28526=CARTESIAN_POINT('Ctrl Pts',(-20.6034922756459,24.8551407643858,-26.978200724581));
#28527=CARTESIAN_POINT('Ctrl Pts',(-20.6021063800053,24.8520065693578,-26.978411266713));
#28528=CARTESIAN_POINT('Ctrl Pts',(-20.5990636132989,24.8450955877511,-26.9788755714642));
#28529=CARTESIAN_POINT('Ctrl Pts',(-20.5974089894626,24.8413178231235,-26.9791294107488));
#28530=CARTESIAN_POINT('Ctrl Pts',(-20.5916595658092,24.8281221219862,-26.9800162000431));
#28531=CARTESIAN_POINT('Ctrl Pts',(-20.5876025676836,24.8186878727369,-26.9806504412069));
#28532=CARTESIAN_POINT('Ctrl Pts',(-20.5467000557884,24.7223053009467,-26.9871326715368));
#28533=CARTESIAN_POINT('Ctrl Pts',(-20.5136514437285,24.6338050129039,-26.9931089683476));
#28534=CARTESIAN_POINT('Ctrl Pts',(-20.4700071163023,24.4991605575395,-27.0022507094504));
#28535=CARTESIAN_POINT('Ctrl Pts',(-20.456461892712,24.4540209799194,-27.0053231697352));
#28536=CARTESIAN_POINT('Ctrl Pts',(-20.4362526953945,24.3808845304795,-27.0103115760106));
#28537=CARTESIAN_POINT('Ctrl Pts',(-20.4289651590741,24.3530660650558,-27.0122113264497));
#28538=CARTESIAN_POINT('Ctrl Pts',(-20.3862460394477,24.180613230437,-27.0239992133313));
#28539=CARTESIAN_POINT('Ctrl Pts',(-20.3605039071274,24.0337714989359,-27.0340954346083));
#28540=CARTESIAN_POINT('Ctrl Pts',(-20.3330041524413,23.7709970912481,-27.0519681521743));
#28541=CARTESIAN_POINT('Ctrl Pts',(-20.3271653359956,23.6557389800221,-27.0597386029792));
#28542=CARTESIAN_POINT('Ctrl Pts',(-20.3276739831064,23.4891930462134,-27.0706769641778));
#28543=CARTESIAN_POINT('Ctrl Pts',(-20.3290513344615,23.4379838597281,-27.0740001600598));
#28544=CARTESIAN_POINT('Ctrl Pts',(-20.3329625754352,23.3609537968624,-27.0789177859605));
#28545=CARTESIAN_POINT('Ctrl Pts',(-20.3345882289384,23.3350970764512,-27.0805546623936));
#28546=CARTESIAN_POINT('Ctrl Pts',(-20.3368491931666,23.3049460358877,-27.0824450548671));
#28547=CARTESIAN_POINT('Ctrl Pts',(-20.3371815178791,23.3006309107382,-27.0827151631127));
#28548=CARTESIAN_POINT('Ctrl Pts',(-20.3377033941646,23.2940282747255,-27.083127774201));
#28549=CARTESIAN_POINT('Ctrl Pts',(-20.3378866970975,23.2917402965951,-27.0832706282321));
#28550=CARTESIAN_POINT('Ctrl Pts',(-20.338208834002,23.2877726522134,-27.0835181343936));
#28551=CARTESIAN_POINT('Ctrl Pts',(-20.3383465409453,23.2860929025797,-27.0836228503175));
#28552=CARTESIAN_POINT('Ctrl Pts',(-20.3386372136275,23.2825811081201,-27.0838416321398));
#28553=CARTESIAN_POINT('Ctrl Pts',(-20.3387904288674,23.2807490912958,-27.0839556834204));
#28554=CARTESIAN_POINT('Ctrl Pts',(-20.3392199648168,23.2756654483533,-27.0842719384555));
#28555=CARTESIAN_POINT('Ctrl Pts',(-20.3394996578835,23.2724140976612,-27.0844739509926));
#28556=CARTESIAN_POINT('Ctrl Pts',(-20.3406266450549,23.2595421896845,-27.0852727167983));
#28557=CARTESIAN_POINT('Ctrl Pts',(-20.3415122555193,23.2499249092361,-27.0858673265037));
#28558=CARTESIAN_POINT('Ctrl Pts',(-20.3576985785761,23.082400492013,-27.0961889709261));
#28559=CARTESIAN_POINT('Ctrl Pts',(-20.3845980169538,22.9258065010839,-27.1052850566293));
#28560=CARTESIAN_POINT('Ctrl Pts',(-20.4804163682251,22.5408641719855,-27.1276378505912));
#28561=CARTESIAN_POINT('Ctrl Pts',(-20.5633040467645,22.3170065845988,-27.1406808360339));
#28562=CARTESIAN_POINT('Ctrl Pts',(-20.7033516195836,22.038045098057,-27.1587878107292));
#28563=CARTESIAN_POINT('Ctrl Pts',(-20.7388964210788,21.9729473214874,-27.1631517063108));
#28564=CARTESIAN_POINT('Ctrl Pts',(-20.7959756707622,21.8764794275465,-27.1698679657483));
#28565=CARTESIAN_POINT('Ctrl Pts',(-20.8158732438125,21.8441672018477,-27.1721615386944));
#28566=CARTESIAN_POINT('Ctrl Pts',(-20.8402917118767,21.8060381767722,-27.1749237051255));
#28567=CARTESIAN_POINT('Ctrl Pts',(-20.8442684038102,21.7998750698024,-27.1753719389211));
#28568=CARTESIAN_POINT('Ctrl Pts',(-20.8504618681525,21.7903479417083,-27.176067590275));
#28569=CARTESIAN_POINT('Ctrl Pts',(-20.852663985154,21.786974383999,-27.1763144586388));
#28570=CARTESIAN_POINT('Ctrl Pts',(-20.8565259857495,21.7810821166994,-27.1767465856523));
#28571=CARTESIAN_POINT('Ctrl Pts',(-20.8581830941586,21.778561586577,-27.1769317398702));
#28572=CARTESIAN_POINT('Ctrl Pts',(-20.8619317185221,21.7728771766915,-27.1773499957243));
#28573=CARTESIAN_POINT('Ctrl Pts',(-20.8640252830125,21.7697146592105,-27.177583174327));
#28574=CARTESIAN_POINT('Ctrl Pts',(-20.8696724100461,21.7612167948402,-27.1782110418472));
#28575=CARTESIAN_POINT('Ctrl Pts',(-20.8732363033976,21.7558883633043,-27.1786061205019));
#28576=CARTESIAN_POINT('Ctrl Pts',(-20.8889486863455,21.7325475397031,-27.1803428628922));
#28577=CARTESIAN_POINT('Ctrl Pts',(-20.9012630200807,21.7146479649917,-27.1816908078596));
#28578=CARTESIAN_POINT('Ctrl Pts',(-20.9211790226122,21.686316749822,-27.1838505169198));
#28579=CARTESIAN_POINT('Ctrl Pts',(-20.9286641508296,21.6758036877424,-27.184657774807));
#28580=CARTESIAN_POINT('Ctrl Pts',(-20.9439858421571,21.6545552562208,-27.1863013473081));
#28581=CARTESIAN_POINT('Ctrl Pts',(-20.9518260710226,21.6438228484408,-27.1871377928967));
#28582=CARTESIAN_POINT('Ctrl Pts',(-20.9606726219819,21.6318688495237,-27.1880765539643));
#28583=CARTESIAN_POINT('Ctrl Pts',(-20.9616138061386,21.6305990188582,-27.1881763654606));
#28584=CARTESIAN_POINT('Ctrl Pts',(-20.9667366158092,21.623698024057,-27.1887192902085));
#28585=CARTESIAN_POINT('Ctrl Pts',(-20.9709356567675,21.6180798644611,-27.1891630702296));
#28586=CARTESIAN_POINT('Ctrl Pts',(-20.9771903562164,21.6097680342387,-27.1898222764186));
#28587=CARTESIAN_POINT('Ctrl Pts',(-20.979231996512,21.6070637988966,-27.1900371660716));
#28588=CARTESIAN_POINT('Ctrl Pts',(-20.9837670935096,21.6010765381762,-27.190513867766));
#28589=CARTESIAN_POINT('Ctrl Pts',(-20.9862625896019,21.597795071282,-27.1907757573389));
#28590=CARTESIAN_POINT('Ctrl Pts',(-20.9936778277722,21.5880830942577,-27.1915527036022));
#28591=CARTESIAN_POINT('Ctrl Pts',(-20.9986154877599,21.581666360853,-27.1920684404946));
#28592=CARTESIAN_POINT('Ctrl Pts',(-21.0258601365433,21.5465353078924,-27.194905322363));
#28593=CARTESIAN_POINT('Ctrl Pts',(-21.0486269763962,21.5181823820836,-27.1972437804498));
#28594=CARTESIAN_POINT('Ctrl Pts',(-21.1137718757252,21.4398077761736,-27.20384668455));
#28595=CARTESIAN_POINT('Ctrl Pts',(-21.1572020062041,21.3906869782413,-27.2081486075978));
#28596=CARTESIAN_POINT('Ctrl Pts',(-21.3604878269591,21.1744313400374,-27.2278261083055));
#28597=CARTESIAN_POINT('Ctrl Pts',(-21.5365383283496,21.0234879716498,-27.2437097035072));
#28598=CARTESIAN_POINT('Ctrl Pts',(-21.7936281069791,20.8471294510117,-27.2644792212185));
#28599=CARTESIAN_POINT('Ctrl Pts',(-21.8617311438462,20.8040731091805,-27.2697723757969));
#28600=CARTESIAN_POINT('Ctrl Pts',(-21.9589654034866,20.7475858510543,-27.2769731829047));
#28601=CARTESIAN_POINT('Ctrl Pts',(-21.9867873873434,20.7319707535634,-27.2789943272813));
#28602=CARTESIAN_POINT('Ctrl Pts',(-22.0188469036213,20.7145982586971,-27.2812748325742));
#28603=CARTESIAN_POINT('Ctrl Pts',(-22.0228605125205,20.7124343602754,-27.2815594750754));
#28604=CARTESIAN_POINT('Ctrl Pts',(-22.028944683598,20.7091707852351,-27.2819896447962));
#28605=CARTESIAN_POINT('Ctrl Pts',(-22.0310118539481,20.708064849308,-27.2821355707));
#28606=CARTESIAN_POINT('Ctrl Pts',(-22.0345724629695,20.7061649183253,-27.2823865244086));
#28607=CARTESIAN_POINT('Ctrl Pts',(-22.0360653183553,20.7053698440847,-27.2824916215947));
#28608=CARTESIAN_POINT('Ctrl Pts',(-22.0391620258546,20.7037237083264,-27.28270938069));
#28609=CARTESIAN_POINT('Ctrl Pts',(-22.0407659670959,20.7028728291535,-27.2828220307546));
#28610=CARTESIAN_POINT('Ctrl Pts',(-22.0446764378578,20.7008025856408,-27.2830963410143));
#28611=CARTESIAN_POINT('Ctrl Pts',(-22.0469837354505,20.6995846633257,-27.2832579087991));
#28612=CARTESIAN_POINT('Ctrl Pts',(-22.0557152412963,20.6949892289551,-27.2838682672576));
#28613=CARTESIAN_POINT('Ctrl Pts',(-22.0621494379016,20.6916305865929,-27.2843158641715));
#28614=CARTESIAN_POINT('Ctrl Pts',(-22.1720690493164,20.6347243806983,-27.2919264069866));
#28615=CARTESIAN_POINT('Ctrl Pts',(-22.278385902341,20.5867990869696,-27.2987445813672));
#28616=CARTESIAN_POINT('Ctrl Pts',(-22.6389719541953,20.4472476424409,-27.3208570302327));
#28617=CARTESIAN_POINT('Ctrl Pts',(-22.9021208458613,20.3818130722391,-27.3354823432333));
#28618=CARTESIAN_POINT('Ctrl Pts',(-23.2523011243991,20.3402444932921,-27.3558338489613));
#28619=CARTESIAN_POINT('Ctrl Pts',(-23.3345807846856,20.3336688280655,-27.3606691824551));
#28620=CARTESIAN_POINT('Ctrl Pts',(-23.4594236850669,20.3285031561878,-27.3681389531905));
#28621=CARTESIAN_POINT('Ctrl Pts',(-23.5018586590562,20.3275864476686,-27.3707009717934));
#28622=CARTESIAN_POINT('Ctrl Pts',(-23.5518681495668,20.327494045324,-27.3737512091903));
#28623=CARTESIAN_POINT('Ctrl Pts',(-23.559438394421,20.3275067319023,-27.3742137742785));
#28624=CARTESIAN_POINT('Ctrl Pts',(-23.5710884201954,20.3275673043312,-27.3749269297939));
#28625=CARTESIAN_POINT('Ctrl Pts',(-23.5751683077212,20.3275962650757,-27.375176925816));
#28626=CARTESIAN_POINT('Ctrl Pts',(-23.5825921627519,20.3276630613571,-27.375632275883));
#28627=CARTESIAN_POINT('Ctrl Pts',(-23.5859361521421,20.3276983544675,-27.3758375498092));
#28628=CARTESIAN_POINT('Ctrl Pts',(-23.5926455178866,20.3277796109207,-27.3762497475168));
#28629=CARTESIAN_POINT('Ctrl Pts',(-23.5960108891255,20.3278256414474,-27.3764566731538));
#28630=CARTESIAN_POINT('Ctrl Pts',(-23.6055488063937,20.3279710426286,-27.3770436139016));
#28631=CARTESIAN_POINT('Ctrl Pts',(-23.6117211230013,20.3280828769112,-27.377424019945));
#28632=CARTESIAN_POINT('Ctrl Pts',(-23.6376193444084,20.3286265600959,-27.3790226005423));
#28633=CARTESIAN_POINT('Ctrl Pts',(-23.6573410603169,20.3292218146726,-27.38024589515));
#28634=CARTESIAN_POINT('Ctrl Pts',(-23.6818738810518,20.3301878376917,-27.3817752713361));
#28635=CARTESIAN_POINT('Ctrl Pts',(-23.6866915886361,20.3303883736123,-27.3820759747956));
#28636=CARTESIAN_POINT('Ctrl Pts',(-23.7033529612528,20.3311193603287,-27.3831171954525));
#28637=CARTESIAN_POINT('Ctrl Pts',(-23.7151940279755,20.3317043476123,-27.3838594173286));
#28638=CARTESIAN_POINT('Ctrl Pts',(-23.7319041231595,20.3326223360048,-27.3849100416364));
#28639=CARTESIAN_POINT('Ctrl Pts',(-23.7367761392773,20.3329010867497,-27.3852167473408));
#28640=CARTESIAN_POINT('Ctrl Pts',(-23.7495874034398,20.3336632764585,-27.3860242645489));
#28641=CARTESIAN_POINT('Ctrl Pts',(-23.7575254910398,20.3341650412033,-27.3865256429478));
#28642=CARTESIAN_POINT('Ctrl Pts',(-23.7723101285133,20.3351545395856,-27.3874613822976));
#28643=CARTESIAN_POINT('Ctrl Pts',(-23.7791571494084,20.3356347705929,-27.3878955091363));
#28644=CARTESIAN_POINT('Ctrl Pts',(-23.7917113942758,20.3365556034639,-27.3886929141803));
#28645=CARTESIAN_POINT('Ctrl Pts',(-23.7974190914475,20.3369895452734,-27.3890559868144));
#28646=CARTESIAN_POINT('Ctrl Pts',(-23.8071130942556,20.3377525374955,-27.3896735499039));
#28647=CARTESIAN_POINT('Ctrl Pts',(-23.8111000133897,20.3380738080876,-27.3899278030432));
#28648=CARTESIAN_POINT('Ctrl Pts',(-23.8198832183645,20.3387980291236,-27.3904885063707));
#28649=CARTESIAN_POINT('Ctrl Pts',(-23.824679214045,20.3392043033286,-27.3907950564591));
#28650=CARTESIAN_POINT('Ctrl Pts',(-23.8502450560752,20.3414277099266,-27.3924312167005));
#28651=CARTESIAN_POINT('Ctrl Pts',(-23.8709974423327,20.3434355861917,-27.3937665279039));
#28652=CARTESIAN_POINT('Ctrl Pts',(-23.9169671777955,20.3483340202737,-27.3967404757581));
#28653=CARTESIAN_POINT('Ctrl Pts',(-23.9421726339419,20.3513214033321,-27.398381835098));
#28654=CARTESIAN_POINT('Ctrl Pts',(-24.2485422030417,20.3913079300507,-27.4184620976162));
#28655=CARTESIAN_POINT('Ctrl Pts',(-24.523653771292,20.4649669869097,-27.4379844135203));
#28656=CARTESIAN_POINT('Ctrl Pts',(-24.825809218905,20.5903579231332,-27.4598164802937));
#28657=CARTESIAN_POINT('Ctrl Pts',(-24.8657629177183,20.6078974098833,-27.4627082128863));
#28658=CARTESIAN_POINT('Ctrl Pts',(-24.9512979700198,20.6475376053584,-27.4688926788763));
#28659=CARTESIAN_POINT('Ctrl Pts',(-24.9967409844313,20.6699133064484,-27.4721743931875));
#28660=CARTESIAN_POINT('Ctrl Pts',(-25.063059387563,20.7045335054178,-27.4769379506344));
#28661=CARTESIAN_POINT('Ctrl Pts',(-25.0843527685705,20.7159558097657,-27.4784634019905));
#28662=CARTESIAN_POINT('Ctrl Pts',(-25.1091375065775,20.7296121273527,-27.4802324490357));
#28663=CARTESIAN_POINT('Ctrl Pts',(-25.1127547636655,20.7316143088887,-27.4804904718943));
#28664=CARTESIAN_POINT('Ctrl Pts',(-25.1183901304226,20.7347477126295,-27.4808921803111));
#28665=CARTESIAN_POINT('Ctrl Pts',(-25.1204108754696,20.7358741473479,-27.4810361720595));
#28666=CARTESIAN_POINT('Ctrl Pts',(-25.1240593781938,20.7379131043381,-27.481296052582));
#28667=CARTESIAN_POINT('Ctrl Pts',(-25.1256875518353,20.7388248619648,-27.4814119901711));
#28668=CARTESIAN_POINT('Ctrl Pts',(-25.1289508605464,20.740656000545,-27.4816442882008));
#28669=CARTESIAN_POINT('Ctrl Pts',(-25.130585978231,20.7415753912655,-27.481760647262));
#28670=CARTESIAN_POINT('Ctrl Pts',(-25.1352252685827,20.7441892960905,-27.4820906898222));
#28671=CARTESIAN_POINT('Ctrl Pts',(-25.1382275366147,20.7458872126071,-27.48230415313));
#28672=CARTESIAN_POINT('Ctrl Pts',(-25.150869962235,20.753063880138,-27.4832025557653));
#28673=CARTESIAN_POINT('Ctrl Pts',(-25.1604846858802,20.7585876289112,-27.4838846181772));
#28674=CARTESIAN_POINT('Ctrl Pts',(-25.1776116016297,20.7685451237803,-27.4850978198798));
#28675=CARTESIAN_POINT('Ctrl Pts',(-25.1851345962312,20.7729599139287,-27.4856301033665));
#28676=CARTESIAN_POINT('Ctrl Pts',(-25.197389025921,20.7802183438603,-27.486496305049));
#28677=CARTESIAN_POINT('Ctrl Pts',(-25.2021311835739,20.7830436576129,-27.4868312942811));
#28678=CARTESIAN_POINT('Ctrl Pts',(-25.3061752250288,20.8453944590595,-27.4941769651038));
#28679=CARTESIAN_POINT('Ctrl Pts',(-25.4022167629854,20.9102229560541,-27.5008772485788));
#28680=CARTESIAN_POINT('Ctrl Pts',(-25.5485161450003,21.0208977144942,-27.5112957396993));
#28681=CARTESIAN_POINT('Ctrl Pts',(-25.6011657139346,21.0633973242185,-27.5150923677892));
#28682=CARTESIAN_POINT('Ctrl Pts',(-25.7522718646537,21.1934377043465,-27.5262476922591));
#28683=CARTESIAN_POINT('Ctrl Pts',(-25.846742002686,21.2853904296058,-27.5335686083081));
#28684=CARTESIAN_POINT('Ctrl Pts',(-26.040334849408,21.4984262833477,-27.5498983373966));
#28685=CARTESIAN_POINT('Ctrl Pts',(-26.1368000453749,21.6214541580965,-27.5589515026325));
#28686=CARTESIAN_POINT('Ctrl Pts',(-26.232501659889,21.7636660968393,-27.5693033675074));
#28687=CARTESIAN_POINT('Ctrl Pts',(-26.2409499253896,21.7764151665385,-27.5702303163041));
#28688=CARTESIAN_POINT('Ctrl Pts',(-26.2554523816259,21.7986424686929,-27.5718447860026));
#28689=CARTESIAN_POINT('Ctrl Pts',(-26.2615483444967,21.8080932245922,-27.5725307361182));
#28690=CARTESIAN_POINT('Ctrl Pts',(-26.2701515405881,21.8215855420155,-27.5735093910273));
#28691=CARTESIAN_POINT('Ctrl Pts',(-26.2726995356101,21.8256011204601,-27.5738005779749));
#28692=CARTESIAN_POINT('Ctrl Pts',(-26.2770731718763,21.8325277092297,-27.5743027235192));
#28693=CARTESIAN_POINT('Ctrl Pts',(-26.278903068152,21.8354360344635,-27.5745135238498));
#28694=CARTESIAN_POINT('Ctrl Pts',(-26.2823900170519,21.8409976912398,-27.5749165687585));
#28695=CARTESIAN_POINT('Ctrl Pts',(-26.284047865499,21.8436505214804,-27.5751087835752));
#28696=CARTESIAN_POINT('Ctrl Pts',(-26.2879106457462,21.8498516773536,-27.5755580256911));
#28697=CARTESIAN_POINT('Ctrl Pts',(-26.2901125423047,21.8534018791974,-27.5758151647898));
#28698=CARTESIAN_POINT('Ctrl Pts',(-26.2976529273765,21.8656124721264,-27.5766993901535));
#28699=CARTESIAN_POINT('Ctrl Pts',(-26.3029572646633,21.8742937870422,-27.5773277324666));
#28700=CARTESIAN_POINT('Ctrl Pts',(-26.3578089267249,21.9650293629311,-27.5838921196927));
#28701=CARTESIAN_POINT('Ctrl Pts',(-26.4037083799335,22.049222229168,-27.5899604577764));
#28702=CARTESIAN_POINT('Ctrl Pts',(-26.4726995227722,22.1904072333082,-27.6001157597815));
#28703=CARTESIAN_POINT('Ctrl Pts',(-26.4980358290127,22.2462400455313,-27.6041261286337));
#28704=CARTESIAN_POINT('Ctrl Pts',(-26.5931479282226,22.472795605622,-27.6203635841559));
#28705=CARTESIAN_POINT('Ctrl Pts',(-26.6498017644445,22.6486366990462,-27.6329121172837));
#28706=CARTESIAN_POINT('Ctrl Pts',(-26.7097274841857,22.9093575789905,-27.6509692449815));
#28707=CARTESIAN_POINT('Ctrl Pts',(-26.7252084198942,22.991070298954,-27.6565486071451));
#28708=CARTESIAN_POINT('Ctrl Pts',(-26.7488938478758,23.1493473482492,-27.6671061356368));
#28709=CARTESIAN_POINT('Ctrl Pts',(-26.7575502042249,23.2257913095039,-27.6720946080847));
#28710=CARTESIAN_POINT('Ctrl Pts',(-26.7640638516621,23.3102623004044,-27.6774340442857));
#28711=CARTESIAN_POINT('Ctrl Pts',(-26.7646357955772,23.3180484247342,-27.677924591551));
#28712=CARTESIAN_POINT('Ctrl Pts',(-26.7655837712384,23.3316288913531,-27.6787772910222));
#28713=CARTESIAN_POINT('Ctrl Pts',(-26.7659724447151,23.3374222745436,-27.6791401278862));
#28714=CARTESIAN_POINT('Ctrl Pts',(-26.766510366941,23.3457783552546,-27.6796621050492));
#28715=CARTESIAN_POINT('Ctrl Pts',(-26.7666722115368,23.3483401872269,-27.6798219500412));
#28716=CARTESIAN_POINT('Ctrl Pts',(-26.7669484020376,23.352796605738,-27.6800996835761));
#28717=CARTESIAN_POINT('Ctrl Pts',(-26.7670641351845,23.3546911022024,-27.6802176508381));
#28718=CARTESIAN_POINT('Ctrl Pts',(-26.7672849326199,23.3583586841663,-27.6804458270211));
#28719=CARTESIAN_POINT('Ctrl Pts',(-26.7673902044812,23.3601317498259,-27.6805560476143));
#28720=CARTESIAN_POINT('Ctrl Pts',(-26.7676379901545,23.3643642765043,-27.6808189460489));
#28721=CARTESIAN_POINT('Ctrl Pts',(-26.7677791500136,23.3668238201183,-27.6809715470843));
#28722=CARTESIAN_POINT('Ctrl Pts',(-26.76819734492,23.3742594091091,-27.6814323748453));
#28723=CARTESIAN_POINT('Ctrl Pts',(-26.7684656594506,23.3792359673273,-27.6817401124202));
#28724=CARTESIAN_POINT('Ctrl Pts',(-26.771087071927,23.4300488404061,-27.6848753945718));
#28725=CARTESIAN_POINT('Ctrl Pts',(-26.7724724436299,23.4759327161919,-27.6876496112822));
#28726=CARTESIAN_POINT('Ctrl Pts',(-26.7728947536254,23.5238210516992,-27.6905001678976));
#28727=CARTESIAN_POINT('Ctrl Pts',(-26.7729104433794,23.5258087595122,-27.6906184057381));
#28728=CARTESIAN_POINT('Ctrl Pts',(-26.7729349638419,23.5293276960502,-27.6908275872599));
#28729=CARTESIAN_POINT('Ctrl Pts',(-26.7729445422572,23.5308589170087,-27.6909185627983));
#28730=CARTESIAN_POINT('Ctrl Pts',(-26.7729781551214,23.536923291716,-27.6912786850976));
#28731=CARTESIAN_POINT('Ctrl Pts',(-26.7729937162975,23.5414565081284,-27.6915474733269));
#28732=CARTESIAN_POINT('Ctrl Pts',(-26.7730009972145,23.5469610462477,-27.6918733737843));
#28733=CARTESIAN_POINT('Ctrl Pts',(-26.7730018428478,23.547932327846,-27.6919308611048));
#28734=CARTESIAN_POINT('Ctrl Pts',(-26.7730307965937,23.6171065457229,-27.6960237967814));
#28735=CARTESIAN_POINT('Ctrl Pts',(-26.7708942687391,23.685297442175,-27.6999698176733));
#28736=CARTESIAN_POINT('Ctrl Pts',(-26.7475149334412,24.0555011632254,-27.7211499751951));
#28737=CARTESIAN_POINT('Ctrl Pts',(-26.6859643129802,24.353425706689,-27.737471870038));
#28738=CARTESIAN_POINT('Ctrl Pts',(-26.5767465221006,24.6578991193774,-27.7564158227598));
#28739=CARTESIAN_POINT('Ctrl Pts',(-26.5695630873687,24.6773330873056,-27.7576345291315));
#28740=CARTESIAN_POINT('Ctrl Pts',(-26.5602633221964,24.701765460286,-27.7591794514905));
#28741=CARTESIAN_POINT('Ctrl Pts',(-26.5583209859049,24.7068298779789,-27.7595003834268));
#28742=CARTESIAN_POINT('Ctrl Pts',(-26.5549015267926,24.715678841402,-27.7600623753962));
#28743=CARTESIAN_POINT('Ctrl Pts',(-26.5534300124923,24.7194655515156,-27.7603032629522));
#28744=CARTESIAN_POINT('Ctrl Pts',(-26.5497758286131,24.7288166070759,-27.7608991089322));
#28745=CARTESIAN_POINT('Ctrl Pts',(-26.547584837468,24.734377667235,-27.7612543242227));
#28746=CARTESIAN_POINT('Ctrl Pts',(-26.5428223863458,24.7463675637165,-27.7620220811712));
#28747=CARTESIAN_POINT('Ctrl Pts',(-26.5402456567134,24.752794263218,-27.76243478686));
#28748=CARTESIAN_POINT('Ctrl Pts',(-26.5347268705365,24.766431437017,-27.7633130779086));
#28749=CARTESIAN_POINT('Ctrl Pts',(-26.5317793532091,24.773639641314,-27.7637788352832));
#28750=CARTESIAN_POINT('Ctrl Pts',(-26.5218520079364,24.7976681626849,-27.7653365908627));
#28751=CARTESIAN_POINT('Ctrl Pts',(-26.5147558308815,24.8144397695091,-27.7664323440683));
#28752=CARTESIAN_POINT('Ctrl Pts',(-26.4989374612271,24.8509603471575,-27.7688375173806));
#28753=CARTESIAN_POINT('Ctrl Pts',(-26.4901582497826,24.8706835099713,-27.7701488040181));
#28754=CARTESIAN_POINT('Ctrl Pts',(-26.4785227033803,24.8961322648778,-27.7718573461241));
#28755=CARTESIAN_POINT('Ctrl Pts',(-26.4758464137888,24.9019399551397,-27.7722483823615));
#28756=CARTESIAN_POINT('Ctrl Pts',(-26.4715567915688,24.9111762406691,-27.7728720813576));
#28757=CARTESIAN_POINT('Ctrl Pts',(-26.4699546570244,24.9146100433308,-27.7731043561075));
#28758=CARTESIAN_POINT('Ctrl Pts',(-26.4670660496595,24.920772712375,-27.773521943844));
#28759=CARTESIAN_POINT('Ctrl Pts',(-26.465781791869,24.9235026171493,-27.7737071797881));
#28760=CARTESIAN_POINT('Ctrl Pts',(-26.4627716175191,24.9298779900951,-27.7741403755748));
#28761=CARTESIAN_POINT('Ctrl Pts',(-26.461042689535,24.9335220237113,-27.7743884398804));
#28762=CARTESIAN_POINT('Ctrl Pts',(-26.4560766090705,24.943938413776,-27.7750988446037));
#28763=CARTESIAN_POINT('Ctrl Pts',(-26.4528226465237,24.9507026855894,-27.775561769883));
#28764=CARTESIAN_POINT('Ctrl Pts',(-26.4317574416837,24.9941038111393,-27.7785423666954));
#28765=CARTESIAN_POINT('Ctrl Pts',(-26.413277202109,25.0304101430023,-27.7810833604011));
#28766=CARTESIAN_POINT('Ctrl Pts',(-26.3562805936072,25.1373227500454,-27.7887131151413));
#28767=CARTESIAN_POINT('Ctrl Pts',(-26.3158065315181,25.206843797112,-27.7938701211423));
#28768=CARTESIAN_POINT('Ctrl Pts',(-26.1912799074142,25.4034356558246,-27.8090332427642));
#28769=CARTESIAN_POINT('Ctrl Pts',(-26.100772022104,25.5261460470135,-27.8192437448183));
#28770=CARTESIAN_POINT('Ctrl Pts',(-25.8523241743234,25.817347432618,-27.8451268344965));
#28771=CARTESIAN_POINT('Ctrl Pts',(-25.6843128591967,25.9761670819324,-27.8608631890206));
#28772=CARTESIAN_POINT('Ctrl Pts',(-25.4901365032949,26.123799971556,-27.8762617352713));
#28773=CARTESIAN_POINT('Ctrl Pts',(-25.4794450245147,26.1318242601176,-27.8771013171008));
#28774=CARTESIAN_POINT('Ctrl Pts',(-25.4657590848714,26.1419634795186,-27.8781652257692));
#28775=CARTESIAN_POINT('Ctrl Pts',(-25.46281072611,26.1441399898598,-27.8783937879586));
#28776=CARTESIAN_POINT('Ctrl Pts',(-25.4581238422539,26.1475875625996,-27.8787561076886));
#28777=CARTESIAN_POINT('Ctrl Pts',(-25.4563877559068,26.1488619112483,-27.8788900951662));
#28778=CARTESIAN_POINT('Ctrl Pts',(-25.45314479405,26.1512373612211,-27.8791399663272));
#28779=CARTESIAN_POINT('Ctrl Pts',(-25.4516382494196,26.1523388865296,-27.8792558794401));
#28780=CARTESIAN_POINT('Ctrl Pts',(-25.4482595072068,26.1548047868761,-27.8795154665618));
#28781=CARTESIAN_POINT('Ctrl Pts',(-25.4463867990182,26.156168449261,-27.8796590902643));
#28782=CARTESIAN_POINT('Ctrl Pts',(-25.4408571949992,26.1601858612588,-27.880082424326));
#28783=CARTESIAN_POINT('Ctrl Pts',(-25.4371961674776,26.1628339550473,-27.8803617405255));
#28784=CARTESIAN_POINT('Ctrl Pts',(-25.4089182331777,26.1831974987447,-27.8825118710273));
#28785=CARTESIAN_POINT('Ctrl Pts',(-25.3840568642563,26.2005731201463,-27.8843595243185));
#28786=CARTESIAN_POINT('Ctrl Pts',(-25.297705981302,26.2591268357333,-27.8906453675226));
#28787=CARTESIAN_POINT('Ctrl Pts',(-25.2350419812564,26.2985392286721,-27.8949815813351));
#28788=CARTESIAN_POINT('Ctrl Pts',(-24.8282243934108,26.5352563772553,-27.9220954164485));
#28789=CARTESIAN_POINT('Ctrl Pts',(-24.4515116493518,26.6697458561519,-27.9430971696385));
#28790=CARTESIAN_POINT('Ctrl Pts',(-24.0415267464132,26.735391284638,-27.968234994199));
#28791=CARTESIAN_POINT('Ctrl Pts',(-24.0232504909872,26.7381565669311,-27.9693589590303));
#28792=CARTESIAN_POINT('Ctrl Pts',(-23.9989970848315,26.7416130670694,-27.9708552936865));
#28793=CARTESIAN_POINT('Ctrl Pts',(-23.9930400876004,26.7424450259339,-27.9712231971251));
#28794=CARTESIAN_POINT('Ctrl Pts',(-23.9837778518436,26.7437121718227,-27.9717958357649));
#28795=CARTESIAN_POINT('Ctrl Pts',(-23.9804741864604,26.7441589179204,-27.9720002045456));
#28796=CARTESIAN_POINT('Ctrl Pts',(-23.9738515274216,26.745044021169,-27.9724101318888));
#28797=CARTESIAN_POINT('Ctrl Pts',(-23.9705325320732,26.745482334314,-27.9726156915776));
#28798=CARTESIAN_POINT('Ctrl Pts',(-23.9631933473753,26.7464399287122,-27.973070510139));
#28799=CARTESIAN_POINT('Ctrl Pts',(-23.9591728539711,26.7469567976377,-27.9733198450236));
#28800=CARTESIAN_POINT('Ctrl Pts',(-23.947509200345,26.7484338964333,-27.9740437053471));
#28801=CARTESIAN_POINT('Ctrl Pts',(-23.939863598296,26.7493743045691,-27.9745188570281));
#28802=CARTESIAN_POINT('Ctrl Pts',(-23.9226111110704,26.7514335941752,-27.9755925577239));
#28803=CARTESIAN_POINT('Ctrl Pts',(-23.913002445059,26.7525366545498,-27.9761916032309));
#28804=CARTESIAN_POINT('Ctrl Pts',(-23.8325928212801,26.761401008441,-27.9812136948862));
#28805=CARTESIAN_POINT('Ctrl Pts',(-23.7615623349881,26.7668559331855,-27.9857090673376));
#28806=CARTESIAN_POINT('Ctrl Pts',(-23.6169160821752,26.7731527285653,-27.9949924779138));
#28807=CARTESIAN_POINT('Ctrl Pts',(-23.5433351847723,26.7738344784115,-27.9997825785216));
#28808=CARTESIAN_POINT('Ctrl Pts',(-23.3009450046869,26.7677815484129,-28.0157712370068));
#28809=CARTESIAN_POINT('Ctrl Pts',(-23.1326943961955,26.7502969351834,-28.0272205050949));
#28810=CARTESIAN_POINT('Ctrl Pts',(-22.7869542469707,26.6866297101573,-28.051001373812));
#28811=CARTESIAN_POINT('Ctrl Pts',(-22.610417657927,26.638328612315,-28.063284995901));
#28812=CARTESIAN_POINT('Ctrl Pts',(-22.4283729664856,26.5714492742446,-28.0755037517968));
#28813=CARTESIAN_POINT('Ctrl Pts',(-22.4178585777924,26.5675240571047,-28.0762077678696));
#28814=CARTESIAN_POINT('Ctrl Pts',(-22.404124386863,26.5623149228752,-28.0771249362809));
#28815=CARTESIAN_POINT('Ctrl Pts',(-22.400886014703,26.5610806873069,-28.0773410166546));
#28816=CARTESIAN_POINT('Ctrl Pts',(-22.3958947294136,26.5591691404018,-28.0776737785532));
#28817=CARTESIAN_POINT('Ctrl Pts',(-22.3941404200447,26.5584955204141,-28.0777906821476));
#28818=CARTESIAN_POINT('Ctrl Pts',(-22.3908197462685,26.5572171137637,-28.0780118619361));
#28819=CARTESIAN_POINT('Ctrl Pts',(-22.3892532733171,26.5566126404994,-28.0781161561847));
#28820=CARTESIAN_POINT('Ctrl Pts',(-22.3856132045299,26.5552047352018,-28.0783584073007));
#28821=CARTESIAN_POINT('Ctrl Pts',(-22.3835399708013,26.5544003822618,-28.0784963074868));
#28822=CARTESIAN_POINT('Ctrl Pts',(-22.3776641046471,26.5521137210949,-28.0788869266434));
#28823=CARTESIAN_POINT('Ctrl Pts',(-22.3738634357685,26.5506263275901,-28.0791393384523));
#28824=CARTESIAN_POINT('Ctrl Pts',(-22.3506953780232,26.5415087080106,-28.0806765125242));
#28825=CARTESIAN_POINT('Ctrl Pts',(-22.3313988845291,26.5336979758403,-28.0819505231964));
#28826=CARTESIAN_POINT('Ctrl Pts',(-22.2737259380351,26.5097004610811,-28.0857432112327));
#28827=CARTESIAN_POINT('Ctrl Pts',(-22.2355848051969,26.4929555953082,-28.088231305606));
#28828=CARTESIAN_POINT('Ctrl Pts',(-22.156442735343,26.4563642927838,-28.0933731878603));
#28829=CARTESIAN_POINT('Ctrl Pts',(-22.1155198733829,26.4363802410779,-28.0960199595268));
#28830=CARTESIAN_POINT('Ctrl Pts',(-22.0750360120315,26.4155367728497,-28.0986394360247));
#28831=CARTESIAN_POINT('Ctrl Pts',(-22.0750360250495,26.4155367795522,-28.3456357132216));
#28832=CARTESIAN_POINT('Ctrl Pts',(-22.091222596573,26.4238705766319,-28.3444667025509));
#28833=CARTESIAN_POINT('Ctrl Pts',(-22.1074805334644,26.4320675962987,-28.3432931375839));
#28834=CARTESIAN_POINT('Ctrl Pts',(-22.3054080929832,26.5297648046258,-28.3290133416339));
#28835=CARTESIAN_POINT('Ctrl Pts',(-22.4950313262397,26.602074816926,-28.3153652355254));
#28836=CARTESIAN_POINT('Ctrl Pts',(-22.8186265216834,26.6916871270874,-28.2926363034063));
#28837=CARTESIAN_POINT('Ctrl Pts',(-22.9491881424434,26.7192608350467,-28.2836204738926));
#28838=CARTESIAN_POINT('Ctrl Pts',(-23.1487073223709,26.7486193460728,-28.2703736691822));
#28839=CARTESIAN_POINT('Ctrl Pts',(-23.2166313515898,26.7564164935814,-28.2659565325146));
#28840=CARTESIAN_POINT('Ctrl Pts',(-23.2957094283846,26.7629532859387,-28.2609595882052));
#28841=CARTESIAN_POINT('Ctrl Pts',(-23.3066661480529,26.7638025950668,-28.2602704704017));
#28842=CARTESIAN_POINT('Ctrl Pts',(-23.3209178774124,26.7648340074414,-28.2593785103852));
#28843=CARTESIAN_POINT('Ctrl Pts',(-23.3242089511216,26.765067106096,-28.2591728395609));
#28844=CARTESIAN_POINT('Ctrl Pts',(-23.3295459451123,26.765436876254,-28.2588398122093));
#28845=CARTESIAN_POINT('Ctrl Pts',(-23.3315916373522,26.7655766491363,-28.2587122805726));
#28846=CARTESIAN_POINT('Ctrl Pts',(-23.3355198921271,26.7658412827015,-28.2584676176437));
#28847=CARTESIAN_POINT('Ctrl Pts',(-23.3374024253794,26.7659664422211,-28.2583504699907));
#28848=CARTESIAN_POINT('Ctrl Pts',(-23.3417323384354,26.7662504959953,-28.2580812576323));
#28849=CARTESIAN_POINT('Ctrl Pts',(-23.3441797964861,26.766408250139,-28.2579292577104));
#28850=CARTESIAN_POINT('Ctrl Pts',(-23.3507095393682,26.766821649096,-28.2575241765232));
#28851=CARTESIAN_POINT('Ctrl Pts',(-23.3547921517343,26.7670723173074,-28.2572713753666));
#28852=CARTESIAN_POINT('Ctrl Pts',(-23.3825577015494,26.7687240399441,-28.2555552154814));
#28853=CARTESIAN_POINT('Ctrl Pts',(-23.4062558144183,26.7698713647319,-28.2541059046928));
#28854=CARTESIAN_POINT('Ctrl Pts',(-23.4328909733259,26.7708661997485,-28.2524921538547));
#28855=CARTESIAN_POINT('Ctrl Pts',(-23.435816843841,26.7709714898925,-28.2523150891112));
#28856=CARTESIAN_POINT('Ctrl Pts',(-23.4447895948412,26.7712821401018,-28.25177270529));
#28857=CARTESIAN_POINT('Ctrl Pts',(-23.4508369528162,26.7714744602716,-28.2514080181906));
#28858=CARTESIAN_POINT('Ctrl Pts',(-23.5565023923831,26.7745370243844,-28.2450503623923));
#28859=CARTESIAN_POINT('Ctrl Pts',(-23.6562100320388,26.772802192418,-28.2392759192138));
#28860=CARTESIAN_POINT('Ctrl Pts',(-23.9963589197518,26.7510753422953,-28.2198714685166));
#28861=CARTESIAN_POINT('Ctrl Pts',(-24.2345453410997,26.7087375037097,-28.2067323379703));
#28862=CARTESIAN_POINT('Ctrl Pts',(-24.5853653927134,26.6047923542932,-28.1857469774809));
#28863=CARTESIAN_POINT('Ctrl Pts',(-24.7027745884231,26.5624543105908,-28.1784394210376));
#28864=CARTESIAN_POINT('Ctrl Pts',(-24.8298160167241,26.5081261618088,-28.1700817451043));
#28865=CARTESIAN_POINT('Ctrl Pts',(-24.8421716834014,26.5027504607126,-28.1692641105389));
#28866=CARTESIAN_POINT('Ctrl Pts',(-24.8608909735119,26.494466074673,-28.1680179181634));
#28867=CARTESIAN_POINT('Ctrl Pts',(-24.8672795384414,26.4916138447798,-28.1675912896985));
#28868=CARTESIAN_POINT('Ctrl Pts',(-24.879047032239,26.4863141217649,-28.1668029860135));
#28869=CARTESIAN_POINT('Ctrl Pts',(-24.88442862512,26.4838725882732,-28.1664415166155));
#28870=CARTESIAN_POINT('Ctrl Pts',(-24.8931250226613,26.4798983076587,-28.1658558379112));
#28871=CARTESIAN_POINT('Ctrl Pts',(-24.8964440077816,26.4783746960102,-28.1656319442895));
#28872=CARTESIAN_POINT('Ctrl Pts',(-24.9028145511808,26.4754371168576,-28.1652014848227));
#28873=CARTESIAN_POINT('Ctrl Pts',(-24.9058665014971,26.4740240067883,-28.1649949488607));
#28874=CARTESIAN_POINT('Ctrl Pts',(-24.9128086315527,26.4707964644134,-28.1645244312726));
#28875=CARTESIAN_POINT('Ctrl Pts',(-24.916697403529,26.4689790348383,-28.1642603460209));
#28876=CARTESIAN_POINT('Ctrl Pts',(-24.9285057280637,26.4634316064408,-28.1634568710614));
#28877=CARTESIAN_POINT('Ctrl Pts',(-24.9364136756692,26.4596771269282,-28.1629166318499));
#28878=CARTESIAN_POINT('Ctrl Pts',(-24.9924176331645,26.4328078055491,-28.1590751908731));
#28879=CARTESIAN_POINT('Ctrl Pts',(-25.0399458663028,26.4085349361942,-28.1557337085104));
#28880=CARTESIAN_POINT('Ctrl Pts',(-25.1033799928596,26.3741268907081,-28.1511587815032));
#28881=CARTESIAN_POINT('Ctrl Pts',(-25.1198334462314,26.3650148724693,-28.1499614442918));
#28882=CARTESIAN_POINT('Ctrl Pts',(-25.1692292808915,26.3370914018397,-28.1463342854025));
#28883=CARTESIAN_POINT('Ctrl Pts',(-25.2019193243432,26.3178423174141,-28.1438896680594));
#28884=CARTESIAN_POINT('Ctrl Pts',(-25.3085456052629,26.2524949138342,-28.1357693187238));
#28885=CARTESIAN_POINT('Ctrl Pts',(-25.3809484801084,26.2039780023688,-28.1300168962215));
#28886=CARTESIAN_POINT('Ctrl Pts',(-25.5000638130591,26.1169627798335,-28.120164061873));
#28887=CARTESIAN_POINT('Ctrl Pts',(-25.5478224245145,26.0799718213193,-28.1161003258449));
#28888=CARTESIAN_POINT('Ctrl Pts',(-25.6814717108706,25.9703094477637,-28.1044255861544));
#28889=CARTESIAN_POINT('Ctrl Pts',(-25.7646361271542,25.8944530915306,-28.0967832329403));
#28890=CARTESIAN_POINT('Ctrl Pts',(-25.9092953044591,25.7479244000381,-28.0829489636283));
#28891=CARTESIAN_POINT('Ctrl Pts',(-25.9720099168832,25.6786177014701,-28.0767379976417));
#28892=CARTESIAN_POINT('Ctrl Pts',(-26.0529830675722,25.5809118788983,-28.0685199261794));
#28893=CARTESIAN_POINT('Ctrl Pts',(-26.0739357864591,25.5548124710593,-28.0663737895877));
#28894=CARTESIAN_POINT('Ctrl Pts',(-26.1053688146291,25.5143841721224,-28.0631296224353));
#28895=CARTESIAN_POINT('Ctrl Pts',(-26.1161430272316,25.5002879979052,-28.0620130314254));
#28896=CARTESIAN_POINT('Ctrl Pts',(-26.1291357384022,25.4829951636764,-28.0606615986522));
#28897=CARTESIAN_POINT('Ctrl Pts',(-26.1314652948904,25.4798828970271,-28.0604190944728));
#28898=CARTESIAN_POINT('Ctrl Pts',(-26.1350933375184,25.4750175382014,-28.0600411225277));
#28899=CARTESIAN_POINT('Ctrl Pts',(-26.1363956748274,25.4732673431353,-28.0599053841224));
#28900=CARTESIAN_POINT('Ctrl Pts',(-26.1386961029975,25.4701692626037,-28.0596655136418));
#28901=CARTESIAN_POINT('Ctrl Pts',(-26.1396949135333,25.4688219275229,-28.0595613308248));
#28902=CARTESIAN_POINT('Ctrl Pts',(-26.1418283757576,25.4659393149201,-28.0593387214288));
#28903=CARTESIAN_POINT('Ctrl Pts',(-26.1429627119285,25.4644038131545,-28.0592203172602));
#28904=CARTESIAN_POINT('Ctrl Pts',(-26.1462401832608,25.4599589836337,-28.0588780740737));
#28905=CARTESIAN_POINT('Ctrl Pts',(-26.1483797993858,25.4570470462781,-28.0586544823067));
#28906=CARTESIAN_POINT('Ctrl Pts',(-26.1578938713649,25.4440530061133,-28.0576594781602));
#28907=CARTESIAN_POINT('Ctrl Pts',(-26.1652147010318,25.4339315006875,-28.0568917651191));
#28908=CARTESIAN_POINT('Ctrl Pts',(-26.2891267691927,25.2605006933438,-28.0438568544211));
#28909=CARTESIAN_POINT('Ctrl Pts',(-26.3902940373637,25.0866676759173,-28.0325809763221));
#28910=CARTESIAN_POINT('Ctrl Pts',(-26.5429088041556,24.7571149001774,-28.0122675951485));
#28911=CARTESIAN_POINT('Ctrl Pts',(-26.5999296419002,24.6047547349596,-28.0032414775938));
#28912=CARTESIAN_POINT('Ctrl Pts',(-26.6834535120523,24.3170490310567,-27.9860561397293));
#28913=CARTESIAN_POINT('Ctrl Pts',(-26.7132381663515,24.1830555833076,-27.9780009853923));
#28914=CARTESIAN_POINT('Ctrl Pts',(-26.7360219800529,24.0371831240379,-27.9690153142882));
#28915=CARTESIAN_POINT('Ctrl Pts',(-26.7375955069498,24.0267744449488,-27.9683730257797));
#28916=CARTESIAN_POINT('Ctrl Pts',(-26.7397875255258,24.0117777377308,-27.9674459538917));
#28917=CARTESIAN_POINT('Ctrl Pts',(-26.7404471835827,24.0071957178688,-27.9671624768382));
#28918=CARTESIAN_POINT('Ctrl Pts',(-26.741576100555,23.9992325907365,-27.9666694249724));
#28919=CARTESIAN_POINT('Ctrl Pts',(-26.742049865516,23.995852121289,-27.9664599933422));
#28920=CARTESIAN_POINT('Ctrl Pts',(-26.7429513243097,23.9893447120259,-27.966056596909));
#28921=CARTESIAN_POINT('Ctrl Pts',(-26.7433797975567,23.9862178824784,-27.9658626570529));
#28922=CARTESIAN_POINT('Ctrl Pts',(-26.7443795968072,23.9788411948198,-27.9654048682809));
#28923=CARTESIAN_POINT('Ctrl Pts',(-26.7449470342126,23.974590823096,-27.9651408964531));
#28924=CARTESIAN_POINT('Ctrl Pts',(-26.7468855769549,23.9598459295181,-27.9642244593242));
#28925=CARTESIAN_POINT('Ctrl Pts',(-26.7482134557164,23.9493458813364,-27.9635706274052));
#28926=CARTESIAN_POINT('Ctrl Pts',(-26.7634633710269,23.823793334209,-27.9557375364648));
#28927=CARTESIAN_POINT('Ctrl Pts',(-26.7712197835639,23.7080907305508,-27.9483637133435));
#28928=CARTESIAN_POINT('Ctrl Pts',(-26.7729215282811,23.5774614639784,-27.9398519451178));
#28929=CARTESIAN_POINT('Ctrl Pts',(-26.773012390264,23.5626892989409,-27.9388867844921));
#28930=CARTESIAN_POINT('Ctrl Pts',(-26.7727575709933,23.2110422962226,-27.9158503389308));
#28931=CARTESIAN_POINT('Ctrl Pts',(-26.7197020955071,22.8763495411284,-27.8922909362946));
#28932=CARTESIAN_POINT('Ctrl Pts',(-26.6152955177309,22.5544455036829,-27.8704582810525));
#28933=CARTESIAN_POINT('Ctrl Pts',(-26.614798743827,22.552917754895,-27.870354689524));
#28934=CARTESIAN_POINT('Ctrl Pts',(-26.6119154340057,22.5440730905102,-27.8697551139629));
#28935=CARTESIAN_POINT('Ctrl Pts',(-26.6095038130355,22.5367643002632,-27.8692602551711));
#28936=CARTESIAN_POINT('Ctrl Pts',(-26.5964312181218,22.4976176123845,-27.8666132174146));
#28937=CARTESIAN_POINT('Ctrl Pts',(-26.5852988693888,22.4659376270967,-27.8644834212579));
#28938=CARTESIAN_POINT('Ctrl Pts',(-26.5719199947845,22.4296861849303,-27.8620652658687));
#28939=CARTESIAN_POINT('Ctrl Pts',(-26.5701558720947,22.4249405702942,-27.8617490864555));
#28940=CARTESIAN_POINT('Ctrl Pts',(-26.5675387330221,22.4179507585522,-27.8612839635613));
#28941=CARTESIAN_POINT('Ctrl Pts',(-26.566694391418,22.4157033555097,-27.8611345028287));
#28942=CARTESIAN_POINT('Ctrl Pts',(-26.5651846726073,22.4116985015733,-27.8608683249617));
#28943=CARTESIAN_POINT('Ctrl Pts',(-26.5645202696188,22.4099406892609,-27.8607515491336));
#28944=CARTESIAN_POINT('Ctrl Pts',(-26.5631185154367,22.4062418509251,-27.8605059430021));
#28945=CARTESIAN_POINT('Ctrl Pts',(-26.5623808275813,22.4043009607798,-27.8603771336885));
#28946=CARTESIAN_POINT('Ctrl Pts',(-26.5604249396263,22.3991698681239,-27.8600367782566));
#28947=CARTESIAN_POINT('Ctrl Pts',(-26.5592035396146,22.3959808756096,-27.8598254253746));
#28948=CARTESIAN_POINT('Ctrl Pts',(-26.5536383735634,22.381519464416,-27.8588677722455));
#28949=CARTESIAN_POINT('Ctrl Pts',(-26.5492362416556,22.370269389447,-27.8581249519048));
#28950=CARTESIAN_POINT('Ctrl Pts',(-26.4445438957539,22.1070886160616,-27.840792771029));
#28951=CARTESIAN_POINT('Ctrl Pts',(-26.3128995881329,21.8687409220148,-27.8260083971645));
#28952=CARTESIAN_POINT('Ctrl Pts',(-26.0642755729425,21.5282726740257,-27.8023801385226));
#28953=CARTESIAN_POINT('Ctrl Pts',(-25.9672458494466,21.4132331838796,-27.7938688589953));
#28954=CARTESIAN_POINT('Ctrl Pts',(-25.8524451970975,21.2949838244306,-27.7841991169555));
#28955=CARTESIAN_POINT('Ctrl Pts',(-25.8422701725874,21.2846437536349,-27.7833453307919));
#28956=CARTESIAN_POINT('Ctrl Pts',(-25.827942769408,21.270279248488,-27.7821473958473));
#28957=CARTESIAN_POINT('Ctrl Pts',(-25.8238487559985,21.266196665622,-27.7818055721336));
#28958=CARTESIAN_POINT('Ctrl Pts',(-25.8169190234892,21.2593233737513,-27.7812277782856));
#28959=CARTESIAN_POINT('Ctrl Pts',(-25.8140890731733,21.2565268495332,-27.780992042157));
#28960=CARTESIAN_POINT('Ctrl Pts',(-25.8036506780703,21.2462498836954,-27.7801233228417));
#28961=CARTESIAN_POINT('Ctrl Pts',(-25.7960103334599,21.2388020563469,-27.77948903373));
#28962=CARTESIAN_POINT('Ctrl Pts',(-25.7854158988804,21.2285766879859,-27.7786115635794));
#28963=CARTESIAN_POINT('Ctrl Pts',(-25.7824932875299,21.2257665220486,-27.7783697169762));
#28964=CARTESIAN_POINT('Ctrl Pts',(-25.7751554492186,21.2187376030999,-27.7777630385599));
#28965=CARTESIAN_POINT('Ctrl Pts',(-25.7707335324531,21.2145258826228,-27.7773979209094));
#28966=CARTESIAN_POINT('Ctrl Pts',(-25.7634265288417,21.2076057209109,-27.7767953487298));
#28967=CARTESIAN_POINT('Ctrl Pts',(-25.7605483641336,21.2048899681197,-27.7765581957637));
#28968=CARTESIAN_POINT('Ctrl Pts',(-25.741055508043,21.1865648233036,-27.7749533329978));
#28969=CARTESIAN_POINT('Ctrl Pts',(-25.7242809224244,21.1711271084033,-27.7735786103019));
#28970=CARTESIAN_POINT('Ctrl Pts',(-25.6954679031304,21.1451695605413,-27.7712271134602));
#28971=CARTESIAN_POINT('Ctrl Pts',(-25.6835122501118,21.1345588326975,-27.7702541946075));
#28972=CARTESIAN_POINT('Ctrl Pts',(-25.6672101433751,21.1203059941518,-27.7689311469195));
#28973=CARTESIAN_POINT('Ctrl Pts',(-25.662932150155,21.1165856411649,-27.7685842831046));
#28974=CARTESIAN_POINT('Ctrl Pts',(-25.656175391532,21.1107408739595,-27.7680369475192));
#28975=CARTESIAN_POINT('Ctrl Pts',(-25.6537031628454,21.1086088922591,-27.7678367898858));
#28976=CARTESIAN_POINT('Ctrl Pts',(-25.6489330379125,21.1045078899317,-27.7674507924296));
#28977=CARTESIAN_POINT('Ctrl Pts',(-25.6466355982512,21.1025383412616,-27.767264974716));
#28978=CARTESIAN_POINT('Ctrl Pts',(-25.6412048158433,21.0978958956884,-27.7668259427331));
#28979=CARTESIAN_POINT('Ctrl Pts',(-25.6380691221251,21.0952257682511,-27.7665726146914));
#28980=CARTESIAN_POINT('Ctrl Pts',(-25.6288988996428,21.0874473526808,-27.7658322430834));
#28981=CARTESIAN_POINT('Ctrl Pts',(-25.6228507127432,21.0823552787908,-27.7653445347762));
#28982=CARTESIAN_POINT('Ctrl Pts',(-25.5788725063078,21.0456049528063,-27.7618025009631));
#28983=CARTESIAN_POINT('Ctrl Pts',(-25.5402394498579,21.0148018571047,-27.7587135933616));
#28984=CARTESIAN_POINT('Ctrl Pts',(-25.4129275838536,20.9179954581738,-27.7485986818957));
#28985=CARTESIAN_POINT('Ctrl Pts',(-25.3215652991524,20.8556686671606,-27.7414344773991));
#28986=CARTESIAN_POINT('Ctrl Pts',(-24.9349558788092,20.6200949718609,-27.7115257856852));
#28987=CARTESIAN_POINT('Ctrl Pts',(-24.6162611888996,20.4897250687589,-27.6875263106363));
#28988=CARTESIAN_POINT('Ctrl Pts',(-24.2806172334618,20.4113528533177,-27.6657409453154));
#28989=CARTESIAN_POINT('Ctrl Pts',(-24.2781867339425,20.4107883121538,-27.6655833814341));
#28990=CARTESIAN_POINT('Ctrl Pts',(-24.2634287327331,20.407378475753,-27.6646278195998));
#28991=CARTESIAN_POINT('Ctrl Pts',(-24.2510849843588,20.4046029149767,-27.6638335165579));
#28992=CARTESIAN_POINT('Ctrl Pts',(-24.2351775371141,20.4011243212991,-27.6628165265227));
#28993=CARTESIAN_POINT('Ctrl Pts',(-24.2316287748377,20.4003545707842,-27.6625900720807));
#28994=CARTESIAN_POINT('Ctrl Pts',(-24.2262088589102,20.3991885424487,-27.6622448701653));
#28995=CARTESIAN_POINT('Ctrl Pts',(-24.2243386561576,20.3987879328969,-27.6621258733536));
#28996=CARTESIAN_POINT('Ctrl Pts',(-24.2206815633181,20.39800796426,-27.6618934148032));
#28997=CARTESIAN_POINT('Ctrl Pts',(-24.2188947155602,20.3976284612798,-27.661779945442));
#28998=CARTESIAN_POINT('Ctrl Pts',(-24.2149636146895,20.3967970395991,-27.6615305508119));
#28999=CARTESIAN_POINT('Ctrl Pts',(-24.2128192285021,20.3963457897579,-27.6613946647799));
#29000=CARTESIAN_POINT('Ctrl Pts',(-24.208369616088,20.3954141823495,-27.6611130228035));
#29001=CARTESIAN_POINT('Ctrl Pts',(-24.2060643191928,20.3949341631727,-27.6609672864054));
#29002=CARTESIAN_POINT('Ctrl Pts',(-24.2001621286091,20.393711930532,-27.660594615446));
#29003=CARTESIAN_POINT('Ctrl Pts',(-24.1965644763096,20.3929733356918,-27.6603678870672));
#29004=CARTESIAN_POINT('Ctrl Pts',(-24.1861607333994,20.3908559840969,-27.659713456821));
#29005=CARTESIAN_POINT('Ctrl Pts',(-24.179351387116,20.3894930631268,-27.6592866420208));
#29006=CARTESIAN_POINT('Ctrl Pts',(-24.0023717711687,20.3546643853969,-27.6482315259105));
#29007=CARTESIAN_POINT('Ctrl Pts',(-23.8297521528159,20.3349618556343,-27.6383561242275));
#29008=CARTESIAN_POINT('Ctrl Pts',(-23.4484967478153,20.3224021052908,-27.6169332664649));
#29009=CARTESIAN_POINT('Ctrl Pts',(-23.2404663162241,20.3356915897079,-27.6054720796417));
#29010=CARTESIAN_POINT('Ctrl Pts',(-22.9156572943151,20.3882810206372,-27.5864908625305));
#29011=CARTESIAN_POINT('Ctrl Pts',(-22.7973442730704,20.4143477497127,-27.5793492315649));
#29012=CARTESIAN_POINT('Ctrl Pts',(-22.6704907839253,20.4498894622086,-27.5713335535967));
#29013=CARTESIAN_POINT('Ctrl Pts',(-22.6602091364746,20.4528254307333,-27.57068130512));
#29014=CARTESIAN_POINT('Ctrl Pts',(-22.64580687572,20.4570156885087,-27.5697639853748));
#29015=CARTESIAN_POINT('Ctrl Pts',(-22.6416737968816,20.4582271768493,-27.5695003134372));
#29016=CARTESIAN_POINT('Ctrl Pts',(-22.6345116909567,20.4603421339048,-27.5690426616133));
#29017=CARTESIAN_POINT('Ctrl Pts',(-22.6314815338907,20.4612417827247,-27.5688488069542));
#29018=CARTESIAN_POINT('Ctrl Pts',(-22.6251851071931,20.4631212660621,-27.5684455108588));
#29019=CARTESIAN_POINT('Ctrl Pts',(-22.6219190611988,20.4641018291953,-27.5682360457735));
#29020=CARTESIAN_POINT('Ctrl Pts',(-22.6142420528619,20.4664199824469,-27.567743049977));
#29021=CARTESIAN_POINT('Ctrl Pts',(-22.6098324002864,20.4677618529782,-27.5674593791032));
#29022=CARTESIAN_POINT('Ctrl Pts',(-22.5954669524367,20.4721669965229,-27.5665336309416));
#29023=CARTESIAN_POINT('Ctrl Pts',(-22.5855232044507,20.4752690544612,-27.5658902802643));
#29024=CARTESIAN_POINT('Ctrl Pts',(-22.4288690561347,20.5249736341063,-27.5557141453052));
#29025=CARTESIAN_POINT('Ctrl Pts',(-22.285690421506,20.5819730215234,-27.5458333273703));
#29026=CARTESIAN_POINT('Ctrl Pts',(-21.9946440933085,20.7227276221636,-27.5244900953961));
#29027=CARTESIAN_POINT('Ctrl Pts',(-21.8482018975906,20.80838630508,-27.5129986719099));
#29028=CARTESIAN_POINT('Ctrl Pts',(-21.5626078206911,21.0071681203855,-27.4894673343863));
#29029=CARTESIAN_POINT('Ctrl Pts',(-21.4247465032278,21.1212093742254,-27.4774738837223));
#29030=CARTESIAN_POINT('Ctrl Pts',(-21.2889783856318,21.2539764858177,-27.4655095693023));
#29031=CARTESIAN_POINT('Ctrl Pts',(-21.280966154777,21.2618942138149,-27.4648029511396));
#29032=CARTESIAN_POINT('Ctrl Pts',(-21.2705396108174,21.2723063939006,-27.4638828823967));
#29033=CARTESIAN_POINT('Ctrl Pts',(-21.268087709431,21.2747628409691,-27.463666481054));
#29034=CARTESIAN_POINT('Ctrl Pts',(-21.264313586221,21.2785561973325,-27.4633333300623));
#29035=CARTESIAN_POINT('Ctrl Pts',(-21.2629885678664,21.2798903011676,-27.4632163575272));
#29036=CARTESIAN_POINT('Ctrl Pts',(-21.2603771441525,21.2825242374737,-27.4629858029898));
#29037=CARTESIAN_POINT('Ctrl Pts',(-21.2590906850647,21.2838239977544,-27.462872216964));
#29038=CARTESIAN_POINT('Ctrl Pts',(-21.2562289940121,21.2867202034551,-27.4626195284817));
#29039=CARTESIAN_POINT('Ctrl Pts',(-21.2546543254948,21.2883171948221,-27.4624804710883));
#29040=CARTESIAN_POINT('Ctrl Pts',(-21.2513809356743,21.2916439279018,-27.46219136977));
#29041=CARTESIAN_POINT('Ctrl Pts',(-21.2496824956679,21.2933739462267,-27.462041348131));
#29042=CARTESIAN_POINT('Ctrl Pts',(-21.2452999143994,21.2978480987988,-27.4616541875922));
#29043=CARTESIAN_POINT('Ctrl Pts',(-21.2426187111102,21.3005951249417,-27.4614172783475));
#29044=CARTESIAN_POINT('Ctrl Pts',(-21.2347966425239,21.3086379214079,-27.4607259564314));
#29045=CARTESIAN_POINT('Ctrl Pts',(-21.229669011587,21.3139466124558,-27.4602725568183));
#29046=CARTESIAN_POINT('Ctrl Pts',(-21.1761827372135,21.3697035767936,-27.4555402873246));
#29047=CARTESIAN_POINT('Ctrl Pts',(-21.1294547676214,21.4216987989674,-27.4513812887903));
#29048=CARTESIAN_POINT('Ctrl Pts',(-21.0363283071697,21.5323604847526,-27.4429387710752));
#29049=CARTESIAN_POINT('Ctrl Pts',(-20.9902068916258,21.5912040813125,-27.4386691064423));
#29050=CARTESIAN_POINT('Ctrl Pts',(-20.7433623807068,21.9297618533628,-27.4149813532217));
#29051=CARTESIAN_POINT('Ctrl Pts',(-20.5864467909286,22.238584460576,-27.3963216915705));
#29052=CARTESIAN_POINT('Ctrl Pts',(-20.4750288076411,22.5861228419328,-27.3742550090276));
#29053=CARTESIAN_POINT('Ctrl Pts',(-20.4688929050841,22.605916875279,-27.3729959150457));
#29054=CARTESIAN_POINT('Ctrl Pts',(-20.4611429728201,22.6317976834487,-27.3713462241427));
#29055=CARTESIAN_POINT('Ctrl Pts',(-20.4593551848093,22.6378322529165,-27.370961328668));
#29056=CARTESIAN_POINT('Ctrl Pts',(-20.4566316490513,22.647125248447,-27.3703682217717));
#29057=CARTESIAN_POINT('Ctrl Pts',(-20.4556833393844,22.6503800023115,-27.3701604214003));
#29058=CARTESIAN_POINT('Ctrl Pts',(-20.4538191165052,22.6568161166219,-27.3697493613167));
#29059=CARTESIAN_POINT('Ctrl Pts',(-20.4529029662033,22.6599974044978,-27.3695461096418));
#29060=CARTESIAN_POINT('Ctrl Pts',(-20.45088326008,22.6670515931156,-27.3690952616911));
#29061=CARTESIAN_POINT('Ctrl Pts',(-20.449782059596,22.6709251574218,-27.3688475889029));
#29062=CARTESIAN_POINT('Ctrl Pts',(-20.4466572488379,22.6819957864979,-27.368139435214));
#29063=CARTESIAN_POINT('Ctrl Pts',(-20.4446514279513,22.6891978073771,-27.3676783752861));
#29064=CARTESIAN_POINT('Ctrl Pts',(-20.432031698148,22.735127460427,-27.3647356193985));
#29065=CARTESIAN_POINT('Ctrl Pts',(-20.4221177325538,22.7740421918965,-27.3622312776528));
#29066=CARTESIAN_POINT('Ctrl Pts',(-20.3948148981791,22.8902477932376,-27.3547162184903));
#29067=CARTESIAN_POINT('Ctrl Pts',(-20.3795469005245,22.9680008883995,-27.3496392843041));
#29068=CARTESIAN_POINT('Ctrl Pts',(-20.3434960960042,23.195676434859,-27.3346300451783));
#29069=CARTESIAN_POINT('Ctrl Pts',(-20.3303887193855,23.346586899906,-27.3244934663298));
#29070=CARTESIAN_POINT('Ctrl Pts',(-20.3247602752572,23.6926575135823,-27.301095174387));
#29071=CARTESIAN_POINT('Ctrl Pts',(-20.3392647210968,23.8873678111172,-27.2878124174258));
#29072=CARTESIAN_POINT('Ctrl Pts',(-20.3730184054975,24.0900803510924,-27.2745017022544));
#29073=CARTESIAN_POINT('Ctrl Pts',(-20.3748179618797,24.1005670473554,-27.2738146778478));
#29074=CARTESIAN_POINT('Ctrl Pts',(-20.383380451811,24.1490230904487,-27.270647948827));
#29075=CARTESIAN_POINT('Ctrl Pts',(-20.3907730311557,24.1868800274762,-27.2681961000597));
#29076=CARTESIAN_POINT('Ctrl Pts',(-20.3998370119586,24.2292386473724,-27.2654846098623));
#29077=CARTESIAN_POINT('Ctrl Pts',(-20.4008404656162,24.2338779634932,-27.265188066928));
#29078=CARTESIAN_POINT('Ctrl Pts',(-20.4023675379607,24.2408634257542,-27.2647422285662));
#29079=CARTESIAN_POINT('Ctrl Pts',(-20.4028835323434,24.2432112049104,-27.2645924984833));
#29080=CARTESIAN_POINT('Ctrl Pts',(-20.4037820055221,24.2472775600696,-27.2643333660178));
#29081=CARTESIAN_POINT('Ctrl Pts',(-20.4041632657479,24.2489963996338,-27.2642238932724));
#29082=CARTESIAN_POINT('Ctrl Pts',(-20.4049525588973,24.2525410362477,-27.2639982647894));
#29083=CARTESIAN_POINT('Ctrl Pts',(-20.4053607726679,24.2543667884236,-27.2638821201531));
#29084=CARTESIAN_POINT('Ctrl Pts',(-20.4063277117511,24.2586738456541,-27.2636082932666));
#29085=CARTESIAN_POINT('Ctrl Pts',(-20.4068877866776,24.2611548536931,-27.2634506892497));
#29086=CARTESIAN_POINT('Ctrl Pts',(-20.4080817631305,24.2664149075113,-27.263116818007));
#29087=CARTESIAN_POINT('Ctrl Pts',(-20.408716416197,24.2691937827882,-27.2629405941249));
#29088=CARTESIAN_POINT('Ctrl Pts',(-20.4104444595008,24.276714168369,-27.2624641079194));
#29089=CARTESIAN_POINT('Ctrl Pts',(-20.4115449083338,24.281454074057,-27.2621642465351));
#29090=CARTESIAN_POINT('Ctrl Pts',(-20.414986669664,24.2961276522568,-27.2612373102804));
#29091=CARTESIAN_POINT('Ctrl Pts',(-20.4173644641279,24.3060528251512,-27.2606122661771));
#29092=CARTESIAN_POINT('Ctrl Pts',(-20.4264149244297,24.3430537504568,-27.2582887618035));
#29093=CARTESIAN_POINT('Ctrl Pts',(-20.4333919821465,24.3700547034005,-27.2566065343163));
#29094=CARTESIAN_POINT('Ctrl Pts',(-20.463100504303,24.4791589201139,-27.2498506205596));
#29095=CARTESIAN_POINT('Ctrl Pts',(-20.4887342817251,24.5604421301773,-27.2449130157355));
#29096=CARTESIAN_POINT('Ctrl Pts',(-20.6187277574231,24.9219992695622,-27.2229963851145));
#29097=CARTESIAN_POINT('Ctrl Pts',(-20.7585553201252,25.187922908098,-27.2068575406488));
#29098=CARTESIAN_POINT('Ctrl Pts',(-20.9453378837994,25.4478776582449,-27.1881204528247));
#29099=CARTESIAN_POINT('Ctrl Pts',(-20.9577988984852,25.4648662199832,-27.1868817434871));
#29100=CARTESIAN_POINT('Ctrl Pts',(-20.9756751268422,25.4887430464348,-27.1851197306153));
#29101=CARTESIAN_POINT('Ctrl Pts',(-20.9809533847627,25.4957334955659,-27.1846012754538));
#29102=CARTESIAN_POINT('Ctrl Pts',(-20.9923596098454,25.5107123575417,-27.1834846887523));
#29103=CARTESIAN_POINT('Ctrl Pts',(-20.998496631977,25.5186937305589,-27.1828862334092));
#29104=CARTESIAN_POINT('Ctrl Pts',(-21.0079814435464,25.5309101037726,-27.1819647670412));
#29105=CARTESIAN_POINT('Ctrl Pts',(-21.011302676566,25.5351657126906,-27.1816427452628));
#29106=CARTESIAN_POINT('Ctrl Pts',(-21.0159069862475,25.5410349076958,-27.181197191485));
#29107=CARTESIAN_POINT('Ctrl Pts',(-21.0171809547537,25.5426556531512,-27.181074002872));
#29108=CARTESIAN_POINT('Ctrl Pts',(-21.0226607669264,25.5496133308452,-27.1805445151488));
#29109=CARTESIAN_POINT('Ctrl Pts',(-21.026881906823,25.5549381486916,-27.1801376376653));
#29110=CARTESIAN_POINT('Ctrl Pts',(-21.0354179279221,25.565636358547,-27.1793168042112));
#29111=CARTESIAN_POINT('Ctrl Pts',(-21.0397332663463,25.5710093382107,-27.1789028319518));
#29112=CARTESIAN_POINT('Ctrl Pts',(-21.0619358400896,25.5984726224765,-27.1767779337644));
#29113=CARTESIAN_POINT('Ctrl Pts',(-21.0800970920959,25.6203388879972,-27.1750563413133));
#29114=CARTESIAN_POINT('Ctrl Pts',(-21.1030807607007,25.6472782177658,-27.1728967126854));
#29115=CARTESIAN_POINT('Ctrl Pts',(-21.1076340105721,25.6525800903421,-27.1724697864939));
#29116=CARTESIAN_POINT('Ctrl Pts',(-21.1150476112965,25.6611560014915,-27.1717761223117));
#29117=CARTESIAN_POINT('Ctrl Pts',(-21.117897421736,25.6644391558828,-27.1715098220131));
#29118=CARTESIAN_POINT('Ctrl Pts',(-21.1229681233152,25.6702570884826,-27.1710365991958));
#29119=CARTESIAN_POINT('Ctrl Pts',(-21.1251863678478,25.6727941734044,-27.1708297871987));
#29120=CARTESIAN_POINT('Ctrl Pts',(-21.1298470893764,25.6781079621941,-27.1703956851505));
#29121=CARTESIAN_POINT('Ctrl Pts',(-21.1322903730021,25.6808839491996,-27.1701683615188));
#29122=CARTESIAN_POINT('Ctrl Pts',(-21.1387018024524,25.6881431950954,-27.1695724772847));
#29123=CARTESIAN_POINT('Ctrl Pts',(-21.142677659514,25.6926195969837,-27.1692035932176));
#29124=CARTESIAN_POINT('Ctrl Pts',(-21.1601949872662,25.7122319408333,-27.1675810738168));
#29125=CARTESIAN_POINT('Ctrl Pts',(-21.1738666514183,25.7272504988128,-27.166321947949));
#29126=CARTESIAN_POINT('Ctrl Pts',(-21.2717601239595,25.8327671696733,-27.1573551654457));
#29127=CARTESIAN_POINT('Ctrl Pts',(-21.3609756864225,25.9184714850618,-27.1494305534831));
#29128=CARTESIAN_POINT('Ctrl Pts',(-21.5751204954169,26.1017256264431,-27.1309314082777));
#29129=CARTESIAN_POINT('Ctrl Pts',(-21.7027636106987,26.1956141639096,-27.1202558090638));
#29130=CARTESIAN_POINT('Ctrl Pts',(-21.9142445350118,26.3283746354195,-27.1033532466859));
#29131=CARTESIAN_POINT('Ctrl Pts',(-21.9937381269423,26.3736798513359,-27.0971618111161));
#29132=CARTESIAN_POINT('Ctrl Pts',(-22.075036065511,26.4155368003841,-27.0910469152906));
#29133=CARTESIAN_POINT('Origin',(-23.5502525316942,23.5502525316942,-77.3107734492734));
#29134=CARTESIAN_POINT('',(-22.0750360129136,26.4155367733039,-25.5932554334314));
#29135=CARTESIAN_POINT('',(-22.0750360153461,26.4155367745563,-25.8427499795855));
#29136=CARTESIAN_POINT('',(-22.0750360153461,26.4155367745563,-77.3107734492734));
#29137=CARTESIAN_POINT('',(-26.7730012222585,23.5532068148341,-26.4393797936538));
#29138=CARTESIAN_POINT('Ctrl Pts',(-22.0750360129136,26.4155367733039,-25.5932554334314));
#29139=CARTESIAN_POINT('Ctrl Pts',(-22.0466160857789,26.400904526575,-25.5952554284658));
#29140=CARTESIAN_POINT('Ctrl Pts',(-22.0184151274967,26.3858501008074,-25.5972702832576));
#29141=CARTESIAN_POINT('Ctrl Pts',(-21.8659511005368,26.3015223303977,-25.6083320059081));
#29142=CARTESIAN_POINT('Ctrl Pts',(-21.7461716184923,26.2245075153379,-25.6176508306857));
#29143=CARTESIAN_POINT('Ctrl Pts',(-21.4613038304606,26.0134772959779,-25.6413397160578));
#29144=CARTESIAN_POINT('Ctrl Pts',(-21.303635164313,25.8705735223199,-25.6559036723081));
#29145=CARTESIAN_POINT('Ctrl Pts',(-21.0944527268427,25.6395215795845,-25.6765955928807));
#29146=CARTESIAN_POINT('Ctrl Pts',(-21.0311771901896,25.5627787652145,-25.6830726758594));
#29147=CARTESIAN_POINT('Ctrl Pts',(-20.9676130371031,25.4779801495591,-25.6897174714637));
#29148=CARTESIAN_POINT('Ctrl Pts',(-20.9636975148505,25.4727232530088,-25.6901273803765));
#29149=CARTESIAN_POINT('Ctrl Pts',(-20.9583104462015,25.4654444387193,-25.6906921223488));
#29150=CARTESIAN_POINT('Ctrl Pts',(-20.956825208201,25.4634327461919,-25.6908479065927));
#29151=CARTESIAN_POINT('Ctrl Pts',(-20.9542831361505,25.4599812165819,-25.6911146791055));
#29152=CARTESIAN_POINT('Ctrl Pts',(-20.9532251579762,25.4585422300046,-25.6912257477665));
#29153=CARTESIAN_POINT('Ctrl Pts',(-20.9511607803285,25.4557295140885,-25.6914425498431));
#29154=CARTESIAN_POINT('Ctrl Pts',(-20.9501542760336,25.4543558701116,-25.6915482903905));
#29155=CARTESIAN_POINT('Ctrl Pts',(-20.9477186181656,25.4510262320079,-25.691804264714));
#29156=CARTESIAN_POINT('Ctrl Pts',(-20.9462905770222,25.4490694184909,-25.6919544201115));
#29157=CARTESIAN_POINT('Ctrl Pts',(-20.941956907097,25.4431170024411,-25.692410333838));
#29158=CARTESIAN_POINT('Ctrl Pts',(-20.939058241125,25.4391163032716,-25.6927156072367));
#29159=CARTESIAN_POINT('Ctrl Pts',(-20.9101819219358,25.3990680971417,-25.6957601621768));
#29160=CARTESIAN_POINT('Ctrl Pts',(-20.8849415955605,25.3624914566933,-25.6984493069875));
#29161=CARTESIAN_POINT('Ctrl Pts',(-20.8147579481775,25.2561459785098,-25.7060455061551));
#29162=CARTESIAN_POINT('Ctrl Pts',(-20.7717398914447,25.1851447816814,-25.7108506896358));
#29163=CARTESIAN_POINT('Ctrl Pts',(-20.6356006970802,24.9395194057876,-25.7268641983878));
#29164=CARTESIAN_POINT('Ctrl Pts',(-20.5558286481992,24.7580144686285,-25.7377197541403));
#29165=CARTESIAN_POINT('Ctrl Pts',(-20.4353490094598,24.3969530827771,-25.759239959292));
#29166=CARTESIAN_POINT('Ctrl Pts',(-20.3923577359698,24.2189910478363,-25.7698177668922));
#29167=CARTESIAN_POINT('Ctrl Pts',(-20.3628658909522,24.0265166909956,-25.7816551154909));
#29168=CARTESIAN_POINT('Ctrl Pts',(-20.3611171214491,24.0146623465175,-25.7823856273575));
#29169=CARTESIAN_POINT('Ctrl Pts',(-20.3587995697496,23.9983217230218,-25.783394695097));
#29170=CARTESIAN_POINT('Ctrl Pts',(-20.3581740435405,23.9938434847684,-25.7836714519002));
#29171=CARTESIAN_POINT('Ctrl Pts',(-20.3571195539444,23.9861764941586,-25.784145650055));
#29172=CARTESIAN_POINT('Ctrl Pts',(-20.3566859360818,23.9829883794347,-25.7843429437593));
#29173=CARTESIAN_POINT('Ctrl Pts',(-20.3558517992045,23.9767859643919,-25.7847269927303));
#29174=CARTESIAN_POINT('Ctrl Pts',(-20.3554507705869,23.9737717355901,-25.7849137316051));
#29175=CARTESIAN_POINT('Ctrl Pts',(-20.3545020456995,23.9665628592628,-25.7853605804908));
#29176=CARTESIAN_POINT('Ctrl Pts',(-20.3539583423078,23.9623677003015,-25.7856208165796));
#29177=CARTESIAN_POINT('Ctrl Pts',(-20.3523831134483,23.9500227526658,-25.7863871852772));
#29178=CARTESIAN_POINT('Ctrl Pts',(-20.3513744929227,23.9418701216849,-25.7868940416044));
#29179=CARTESIAN_POINT('Ctrl Pts',(-20.3433305143562,23.8747458198268,-25.7910734740989));
#29180=CARTESIAN_POINT('Ctrl Pts',(-20.3378957416415,23.8155972373785,-25.7947963390178));
#29181=CARTESIAN_POINT('Ctrl Pts',(-20.3285759293287,23.6701510508368,-25.8040577793937));
#29182=CARTESIAN_POINT('Ctrl Pts',(-20.3265203635264,23.5837865669375,-25.8096498790746));
#29183=CARTESIAN_POINT('Ctrl Pts',(-20.3312443887873,23.2955008810514,-25.8286127636319));
#29184=CARTESIAN_POINT('Ctrl Pts',(-20.3535312457334,23.0943235734584,-25.8423650085166));
#29185=CARTESIAN_POINT('Ctrl Pts',(-20.4268977295717,22.7401297703474,-25.8667698532619));
#29186=CARTESIAN_POINT('Ctrl Pts',(-20.4708981446793,22.5862844333187,-25.8774245470127));
#29187=CARTESIAN_POINT('Ctrl Pts',(-20.5293837507614,22.4275069688881,-25.8880659182035));
#29188=CARTESIAN_POINT('Ctrl Pts',(-20.5326689630047,22.4187070391859,-25.8886544743528));
#29189=CARTESIAN_POINT('Ctrl Pts',(-20.5371344159718,22.4069034181398,-25.8894421585468));
#29190=CARTESIAN_POINT('Ctrl Pts',(-20.5382807193698,22.4038870678297,-25.8896432916494));
#29191=CARTESIAN_POINT('Ctrl Pts',(-20.5400845987286,22.3991617747834,-25.889958129409));
#29192=CARTESIAN_POINT('Ctrl Pts',(-20.5407391001022,22.3974516727391,-25.8900720191904));
#29193=CARTESIAN_POINT('Ctrl Pts',(-20.5419994419277,22.3941669999518,-25.8902906728358));
#29194=CARTESIAN_POINT('Ctrl Pts',(-20.5426050573807,22.3925923574354,-25.890395449145));
#29195=CARTESIAN_POINT('Ctrl Pts',(-20.5440429341088,22.3888625216875,-25.8906435273757));
#29196=CARTESIAN_POINT('Ctrl Pts',(-20.5448762757092,22.3867077495736,-25.8907867630043));
#29197=CARTESIAN_POINT('Ctrl Pts',(-20.5473027640423,22.3804535752124,-25.8912022672793));
#29198=CARTESIAN_POINT('Ctrl Pts',(-20.5489019943193,22.3763565150168,-25.8914741690518));
#29199=CARTESIAN_POINT('Ctrl Pts',(-20.5596986649789,22.3488628679761,-25.8932969084707));
#29200=CARTESIAN_POINT('Ctrl Pts',(-20.5691615391037,22.3255704743457,-25.8948319705014));
#29201=CARTESIAN_POINT('Ctrl Pts',(-20.5992255527518,22.2539833284593,-25.8995285319187));
#29202=CARTESIAN_POINT('Ctrl Pts',(-20.6207358953281,22.2060773081627,-25.9026412468845));
#29203=CARTESIAN_POINT('Ctrl Pts',(-20.7266384798453,21.9848526626355,-25.9169691570747));
#29204=CARTESIAN_POINT('Ctrl Pts',(-20.8253061598993,21.8187926760373,-25.9276078750564));
#29205=CARTESIAN_POINT('Ctrl Pts',(-21.075301156244,21.4728763016167,-25.9514974228584));
#29206=CARTESIAN_POINT('Ctrl Pts',(-21.2325934954969,21.298739857563,-25.9647842345868));
#29207=CARTESIAN_POINT('Ctrl Pts',(-21.4188107304198,21.1329587006397,-25.9799075518166));
#29208=CARTESIAN_POINT('Ctrl Pts',(-21.4303589499629,21.1228249205734,-25.9808428965056));
#29209=CARTESIAN_POINT('Ctrl Pts',(-21.4461973801844,21.1091256221012,-25.9821224904774));
#29210=CARTESIAN_POINT('Ctrl Pts',(-21.4504251679843,21.1054879803865,-25.9824637443543));
#29211=CARTESIAN_POINT('Ctrl Pts',(-21.4571285021402,21.0997505633829,-25.9830043350012));
#29212=CARTESIAN_POINT('Ctrl Pts',(-21.4595978284044,21.0976435104106,-25.983203371009));
#29213=CARTESIAN_POINT('Ctrl Pts',(-21.4643789991388,21.0935762494489,-25.983588552876));
#29214=CARTESIAN_POINT('Ctrl Pts',(-21.4666904348543,21.0916155641702,-25.9837746788138));
#29215=CARTESIAN_POINT('Ctrl Pts',(-21.4721801403489,21.086972199082,-25.9842165239373));
#29216=CARTESIAN_POINT('Ctrl Pts',(-21.475360838293,21.0842924101387,-25.9844723613647));
#29217=CARTESIAN_POINT('Ctrl Pts',(-21.4819520062175,21.078761026196,-25.9850021822777));
#29218=CARTESIAN_POINT('Ctrl Pts',(-21.4853632051681,21.0759103172223,-25.9852762012896));
#29219=CARTESIAN_POINT('Ctrl Pts',(-21.5044794001666,21.0600021423594,-25.986810771898));
#29220=CARTESIAN_POINT('Ctrl Pts',(-21.5203020622721,21.0470873817229,-25.9880771181759));
#29221=CARTESIAN_POINT('Ctrl Pts',(-21.5618579938909,21.0138217640207,-25.9913936382917));
#29222=CARTESIAN_POINT('Ctrl Pts',(-21.5877806383283,20.9937123273048,-25.9934533155369));
#29223=CARTESIAN_POINT('Ctrl Pts',(-21.7038148360023,20.9065038095629,-26.0026352737741));
#29224=CARTESIAN_POINT('Ctrl Pts',(-21.797083216875,20.8437544101364,-26.0099213445031));
#29225=CARTESIAN_POINT('Ctrl Pts',(-22.0284305272443,20.7050902457756,-26.0277530298547));
#29226=CARTESIAN_POINT('Ctrl Pts',(-22.1691708408958,20.6341768044259,-26.0384172166561));
#29227=CARTESIAN_POINT('Ctrl Pts',(-22.4863892306049,20.5024755421486,-26.0616561809228));
#29228=CARTESIAN_POINT('Ctrl Pts',(-22.6641432575376,20.4461297931122,-26.0741841150298));
#29229=CARTESIAN_POINT('Ctrl Pts',(-22.8568016817507,20.4029726116038,-26.0866236460597));
#29230=CARTESIAN_POINT('Ctrl Pts',(-22.8678295755585,20.4005630399126,-26.0873317600395));
#29231=CARTESIAN_POINT('Ctrl Pts',(-22.8822673444627,20.3974878057661,-26.0882534838102));
#29232=CARTESIAN_POINT('Ctrl Pts',(-22.885665780598,20.3967696828498,-26.0884700575069));
#29233=CARTESIAN_POINT('Ctrl Pts',(-22.8909061585447,20.3956711870409,-26.0888034110007));
#29234=CARTESIAN_POINT('Ctrl Pts',(-22.8927472699457,20.3952869327319,-26.0889204141328));
#29235=CARTESIAN_POINT('Ctrl Pts',(-22.8962325141349,20.3945627183802,-26.0891416842019));
#29236=CARTESIAN_POINT('Ctrl Pts',(-22.8978765679066,20.3942224331177,-26.0892459693726));
#29237=CARTESIAN_POINT('Ctrl Pts',(-22.9016964896863,20.3934349004004,-26.0894880603117));
#29238=CARTESIAN_POINT('Ctrl Pts',(-22.903872551095,20.3929886184895,-26.0896258096721));
#29239=CARTESIAN_POINT('Ctrl Pts',(-22.9083523754007,20.3920746903083,-26.0899090652074));
#29240=CARTESIAN_POINT('Ctrl Pts',(-22.9106561928953,20.3916073138913,-26.0900545557954));
#29241=CARTESIAN_POINT('Ctrl Pts',(-22.9223004883275,20.3892582927471,-26.0907890267353));
#29242=CARTESIAN_POINT('Ctrl Pts',(-22.9316488971708,20.38741553049,-26.0913757932439));
#29243=CARTESIAN_POINT('Ctrl Pts',(-23.031887606566,20.3681178628545,-26.0976378217376));
#29244=CARTESIAN_POINT('Ctrl Pts',(-23.1234912616387,20.3545426362438,-26.1031002694851));
#29245=CARTESIAN_POINT('Ctrl Pts',(-23.36549370013,20.3292734116293,-26.1171488011011));
#29246=CARTESIAN_POINT('Ctrl Pts',(-23.5163487217757,20.3241560729969,-26.1255285187324));
#29247=CARTESIAN_POINT('Ctrl Pts',(-23.8323603099707,20.3356129472515,-26.1432025886247));
#29248=CARTESIAN_POINT('Ctrl Pts',(-23.9969887292421,20.3543312104419,-26.1524859298898));
#29249=CARTESIAN_POINT('Ctrl Pts',(-24.2533264134514,20.4036757062538,-26.1677018267937));
#29250=CARTESIAN_POINT('Ctrl Pts',(-24.3463526069307,20.4259157198697,-26.1733833970995));
#29251=CARTESIAN_POINT('Ctrl Pts',(-24.4480199986554,20.4550571408937,-26.1798212244726));
#29252=CARTESIAN_POINT('Ctrl Pts',(-24.4577801060651,20.4579047779642,-26.1804415992924));
#29253=CARTESIAN_POINT('Ctrl Pts',(-24.4715302085239,20.461987250421,-26.181318947267));
#29254=CARTESIAN_POINT('Ctrl Pts',(-24.4755315993695,20.4631837517677,-26.1815746650283));
#29255=CARTESIAN_POINT('Ctrl Pts',(-24.4825257580295,20.4652899746741,-26.1820223507182));
#29256=CARTESIAN_POINT('Ctrl Pts',(-24.4855195550988,20.4661962835715,-26.1822142065693));
#29257=CARTESIAN_POINT('Ctrl Pts',(-24.4917995457593,20.4681074034527,-26.1826171357466));
#29258=CARTESIAN_POINT('Ctrl Pts',(-24.4950854591017,20.4691131141441,-26.1828282383828));
#29259=CARTESIAN_POINT('Ctrl Pts',(-24.5029163974237,20.4715236134287,-26.1833319959671));
#29260=CARTESIAN_POINT('Ctrl Pts',(-24.5074599231468,20.4729332108256,-26.1836248086719));
#29261=CARTESIAN_POINT('Ctrl Pts',(-24.5170340081362,20.4759267593049,-26.1842429499482));
#29262=CARTESIAN_POINT('Ctrl Pts',(-24.5220638291835,20.4775130081565,-26.1845683535597));
#29263=CARTESIAN_POINT('Ctrl Pts',(-24.5631955841039,20.4905957771221,-26.1872347919139));
#29264=CARTESIAN_POINT('Ctrl Pts',(-24.5990948177383,20.5027153712128,-26.1895963136385));
#29265=CARTESIAN_POINT('Ctrl Pts',(-24.7044609709276,20.5403692459345,-26.1966327866888));
#29266=CARTESIAN_POINT('Ctrl Pts',(-24.7732675739397,20.5676651825905,-26.2013652384361));
#29267=CARTESIAN_POINT('Ctrl Pts',(-24.9350324553696,20.6383771541438,-26.2128267337714));
#29268=CARTESIAN_POINT('Ctrl Pts',(-25.0269740096375,20.6839091609418,-26.2196164624709));
#29269=CARTESIAN_POINT('Ctrl Pts',(-25.1924470295556,20.7759327578964,-26.2323069832667));
#29270=CARTESIAN_POINT('Ctrl Pts',(-25.2665739945196,20.8211697425376,-26.2381787127077));
#29271=CARTESIAN_POINT('Ctrl Pts',(-25.5088286091214,20.9827863629253,-26.2578918473817));
#29272=CARTESIAN_POINT('Ctrl Pts',(-25.6677170236228,21.1121657469431,-26.2717348321048));
#29273=CARTESIAN_POINT('Ctrl Pts',(-25.821858189922,21.2641925738402,-26.2853852131768));
#29274=CARTESIAN_POINT('Ctrl Pts',(-25.8303793546975,21.2726915381514,-26.2861405184911));
#29275=CARTESIAN_POINT('Ctrl Pts',(-25.8413604848419,21.2837674567762,-26.2871145266407));
#29276=CARTESIAN_POINT('Ctrl Pts',(-25.8438639208011,21.2863008882499,-26.2873366217572));
#29277=CARTESIAN_POINT('Ctrl Pts',(-25.8476953866011,21.2901911397318,-26.2876765952293));
#29278=CARTESIAN_POINT('Ctrl Pts',(-25.8490264155081,21.2915449813149,-26.2877947113037));
#29279=CARTESIAN_POINT('Ctrl Pts',(-25.8516493791459,21.2942176203209,-26.2880274949857));
#29280=CARTESIAN_POINT('Ctrl Pts',(-25.8529413702411,21.2955363447514,-26.2881421668035));
#29281=CARTESIAN_POINT('Ctrl Pts',(-25.8558175709315,21.298477109276,-26.288397468802));
#29282=CARTESIAN_POINT('Ctrl Pts',(-25.8574011985168,21.3000997074586,-26.2885380526686));
#29283=CARTESIAN_POINT('Ctrl Pts',(-25.8606679701239,21.3034539435115,-26.2888280899896));
#29284=CARTESIAN_POINT('Ctrl Pts',(-25.8623508835512,21.3051858054197,-26.2889775252629));
#29285=CARTESIAN_POINT('Ctrl Pts',(-25.8666881331037,21.3096592556299,-26.2893627090665));
#29286=CARTESIAN_POINT('Ctrl Pts',(-25.8693395588278,21.3124036795251,-26.2895982312024));
#29287=CARTESIAN_POINT('Ctrl Pts',(-25.9037394696299,21.3481369526412,-26.292654723985));
#29288=CARTESIAN_POINT('Ctrl Pts',(-25.93478833906,21.3817960983765,-26.2954223621426));
#29289=CARTESIAN_POINT('Ctrl Pts',(-26.0353763748323,21.4956149352642,-26.3044645540959));
#29290=CARTESIAN_POINT('Ctrl Pts',(-26.101678464393,21.578551275761,-26.3105516153088));
#29291=CARTESIAN_POINT('Ctrl Pts',(-26.1877841110832,21.6978948818709,-26.3188719448097));
#29292=CARTESIAN_POINT('Ctrl Pts',(-26.2111581172451,21.7316312805218,-26.3211782084304));
#29293=CARTESIAN_POINT('Ctrl Pts',(-26.2578370083805,21.8018316399261,-26.3259025378353));
#29294=CARTESIAN_POINT('Ctrl Pts',(-26.2810645145316,21.8383368609585,-26.3283193986257));
#29295=CARTESIAN_POINT('Ctrl Pts',(-26.4412065254279,22.1015791237185,-26.3455359781616));
#29296=CARTESIAN_POINT('Ctrl Pts',(-26.5504225488228,22.3439262135446,-26.3603971229294));
#29297=CARTESIAN_POINT('Ctrl Pts',(-26.6336827338814,22.612781136021,-26.3774560674618));
#29298=CARTESIAN_POINT('Ctrl Pts',(-26.6384817946835,22.6287133667779,-26.3784685467288));
#29299=CARTESIAN_POINT('Ctrl Pts',(-26.644776610432,22.6502128086864,-26.3798371630166));
#29300=CARTESIAN_POINT('Ctrl Pts',(-26.6463811801509,22.6557481055433,-26.3801897385123));
#29301=CARTESIAN_POINT('Ctrl Pts',(-26.6488765163352,22.6644434419306,-26.3807439323971));
#29302=CARTESIAN_POINT('Ctrl Pts',(-26.6497773216551,22.6676006082332,-26.3809452227713));
#29303=CARTESIAN_POINT('Ctrl Pts',(-26.6514978781004,22.673665973772,-26.3813320660291));
#29304=CARTESIAN_POINT('Ctrl Pts',(-26.6523183672854,22.6765739616839,-26.3815175946163));
#29305=CARTESIAN_POINT('Ctrl Pts',(-26.6542369828561,22.6834107176471,-26.3819539199041));
#29306=CARTESIAN_POINT('Ctrl Pts',(-26.6553317398057,22.6873404187035,-26.3822048260951));
#29307=CARTESIAN_POINT('Ctrl Pts',(-26.6575744862882,22.6954504341637,-26.3827228721671));
#29308=CARTESIAN_POINT('Ctrl Pts',(-26.658721507635,22.6996310055359,-26.3829900430241));
#29309=CARTESIAN_POINT('Ctrl Pts',(-26.661656323595,22.7104127977774,-26.3836794166359));
#29310=CARTESIAN_POINT('Ctrl Pts',(-26.6634315399716,22.7170173931024,-26.3841020278085));
#29311=CARTESIAN_POINT('Ctrl Pts',(-26.6776328213054,22.7705314330652,-26.3875289299324));
#29312=CARTESIAN_POINT('Ctrl Pts',(-26.6890183623401,22.8177082581051,-26.3905667834484));
#29313=CARTESIAN_POINT('Ctrl Pts',(-26.7485255020659,23.091222376041,-26.4082874827796));
#29314=CARTESIAN_POINT('Ctrl Pts',(-26.7732131713021,23.321914293925,-26.4237303520041));
#29315=CARTESIAN_POINT('Ctrl Pts',(-26.7730011780047,23.5532063773351,-26.4393798414846));
#29316=CARTESIAN_POINT('Ctrl Pts',(-26.7730011776085,23.5532068095779,-26.4393798707307));
#29317=CARTESIAN_POINT('Ctrl Pts',(-26.7728187939646,23.7521646139568,-26.4528415856483));
#29318=CARTESIAN_POINT('Ctrl Pts',(-26.7542127905816,23.9507015891791,-26.4663742124312));
#29319=CARTESIAN_POINT('Ctrl Pts',(-26.7116066042551,24.1771034647024,-26.4811392033754));
#29320=CARTESIAN_POINT('Ctrl Pts',(-26.7053548002584,24.2078477869537,-26.4831290045788));
#29321=CARTESIAN_POINT('Ctrl Pts',(-26.6978017852289,24.2423993461137,-26.4853442721287));
#29322=CARTESIAN_POINT('Ctrl Pts',(-26.6969415319832,24.2462998375609,-26.4855940493224));
#29323=CARTESIAN_POINT('Ctrl Pts',(-26.6955333286218,24.2526288330179,-26.4859988394831));
#29324=CARTESIAN_POINT('Ctrl Pts',(-26.6949898153863,24.2550583041157,-26.4861541035073));
#29325=CARTESIAN_POINT('Ctrl Pts',(-26.6939341498047,24.2597515333118,-26.4864538054994));
#29326=CARTESIAN_POINT('Ctrl Pts',(-26.6934223662965,24.2620153715993,-26.4865982645441));
#29327=CARTESIAN_POINT('Ctrl Pts',(-26.6924945752026,24.2660988746399,-26.4868586454711));
#29328=CARTESIAN_POINT('Ctrl Pts',(-26.692079433339,24.2679187262862,-26.4869746170569));
#29329=CARTESIAN_POINT('Ctrl Pts',(-26.6911826369063,24.2718343085429,-26.4872239906468));
#29330=CARTESIAN_POINT('Ctrl Pts',(-26.6907004671745,24.2739299122374,-26.4873573620492));
#29331=CARTESIAN_POINT('Ctrl Pts',(-26.6893940226746,24.279582080404,-26.4877168401273));
#29332=CARTESIAN_POINT('Ctrl Pts',(-26.6885657981603,24.2831377429326,-26.4879427182525));
#29333=CARTESIAN_POINT('Ctrl Pts',(-26.6847072690303,24.2995763701924,-26.4889858231773));
#29334=CARTESIAN_POINT('Ctrl Pts',(-26.6816036104003,24.3124422400324,-26.4897988653303));
#29335=CARTESIAN_POINT('Ctrl Pts',(-26.6259159983002,24.5372061696567,-26.5039495852026));
#29336=CARTESIAN_POINT('Ctrl Pts',(-26.5520031509013,24.7432775469653,-26.5161201670329));
#29337=CARTESIAN_POINT('Ctrl Pts',(-26.4375640099535,24.9826461329155,-26.530945810762));
#29338=CARTESIAN_POINT('Ctrl Pts',(-26.4164043658069,25.0245295185153,-26.5335660783988));
#29339=CARTESIAN_POINT('Ctrl Pts',(-26.3723481959893,25.1071981816068,-26.5388134831348));
#29340=CARTESIAN_POINT('Ctrl Pts',(-26.3494634076132,25.1479765534623,-26.5414399236056));
#29341=CARTESIAN_POINT('Ctrl Pts',(-26.2569383071893,25.3047532254069,-26.5517267163221));
#29342=CARTESIAN_POINT('Ctrl Pts',(-26.1809153902179,25.4168075921755,-26.5594982311706));
#29343=CARTESIAN_POINT('Ctrl Pts',(-26.0639810361362,25.5677727300214,-26.570840231124));
#29344=CARTESIAN_POINT('Ctrl Pts',(-26.0287459242314,25.6109050170868,-26.5741893002898));
#29345=CARTESIAN_POINT('Ctrl Pts',(-25.9886642750751,25.6574541673798,-26.577934422271));
#29346=CARTESIAN_POINT('Ctrl Pts',(-25.9849042592158,25.6617973521273,-26.5782851409547));
#29347=CARTESIAN_POINT('Ctrl Pts',(-25.9777882968403,25.669972706456,-26.5789477591288));
#29348=CARTESIAN_POINT('Ctrl Pts',(-25.9744348340489,25.6738070223618,-26.5792595548606));
#29349=CARTESIAN_POINT('Ctrl Pts',(-25.9687599733586,25.6802646414454,-26.5797864056087));
#29350=CARTESIAN_POINT('Ctrl Pts',(-25.9664433555826,25.6828921485719,-26.5800012604653));
#29351=CARTESIAN_POINT('Ctrl Pts',(-25.961852048035,25.6880825244253,-26.5804266527004));
#29352=CARTESIAN_POINT('Ctrl Pts',(-25.9595775450603,25.6906455528128,-26.5806371820813));
#29353=CARTESIAN_POINT('Ctrl Pts',(-25.954557091364,25.6962847191884,-26.5811014256582));
#29354=CARTESIAN_POINT('Ctrl Pts',(-25.9518093188138,25.6993592213221,-26.5813552164458));
#29355=CARTESIAN_POINT('Ctrl Pts',(-25.942200720708,25.7100689106365,-26.5822416627262));
#29356=CARTESIAN_POINT('Ctrl Pts',(-25.9353093782173,25.7176765245055,-26.5828756080392));
#29357=CARTESIAN_POINT('Ctrl Pts',(-25.8647669544663,25.7948071564964,-26.589346795019));
#29358=CARTESIAN_POINT('Ctrl Pts',(-25.79813719248,25.8615322686978,-26.5953118672348));
#29359=CARTESIAN_POINT('Ctrl Pts',(-25.603024202773,26.0404978431804,-26.6124106714986));
#29360=CARTESIAN_POINT('Ctrl Pts',(-25.4684291804516,26.1455903907483,-26.6238087826733));
#29361=CARTESIAN_POINT('Ctrl Pts',(-25.2306108965602,26.3026382741286,-26.6430725027435));
#29362=CARTESIAN_POINT('Ctrl Pts',(-25.1317542002661,26.3606056611473,-26.6508504791865));
#29363=CARTESIAN_POINT('Ctrl Pts',(-24.9445148763404,26.4573842054219,-26.664973187452));
#29364=CARTESIAN_POINT('Ctrl Pts',(-24.8570639945482,26.4977309699153,-26.6713408444356));
#29365=CARTESIAN_POINT('Ctrl Pts',(-24.7354057767133,26.5473783905949,-26.6797764110105));
#29366=CARTESIAN_POINT('Ctrl Pts',(-24.7026640372419,26.5601195723894,-26.6820060338804));
#29367=CARTESIAN_POINT('Ctrl Pts',(-24.6664360610661,26.5735395089644,-26.6844235475585));
#29368=CARTESIAN_POINT('Ctrl Pts',(-24.6631512467908,26.5747502203004,-26.6846423006544));
#29369=CARTESIAN_POINT('Ctrl Pts',(-24.6577215003067,26.576741463756,-26.6850031545402));
#29370=CARTESIAN_POINT('Ctrl Pts',(-24.6555777105048,26.5775250700522,-26.6851454373212));
#29371=CARTESIAN_POINT('Ctrl Pts',(-24.6513917103602,26.5790501135761,-26.6854228864567));
#29372=CARTESIAN_POINT('Ctrl Pts',(-24.6493495798175,26.5797917642642,-26.6855580655519));
#29373=CARTESIAN_POINT('Ctrl Pts',(-24.6457299551105,26.5811021797688,-26.6857973571994));
#29374=CARTESIAN_POINT('Ctrl Pts',(-24.6441527757854,26.5816717752915,-26.6859015194632));
#29375=CARTESIAN_POINT('Ctrl Pts',(-24.6407727611106,26.5828894802824,-26.6861245239524));
#29376=CARTESIAN_POINT('Ctrl Pts',(-24.638969797323,26.5835372114232,-26.6862433430584));
#29377=CARTESIAN_POINT('Ctrl Pts',(-24.633732624901,26.5854134422677,-26.6865880927255));
#29378=CARTESIAN_POINT('Ctrl Pts',(-24.6302968927519,26.5866377252935,-26.6868137702857));
#29379=CARTESIAN_POINT('Ctrl Pts',(-24.6147953716523,26.5921318716312,-26.6878298272367));
#29380=CARTESIAN_POINT('Ctrl Pts',(-24.6027060719757,26.596335743839,-26.6886163132033));
#29381=CARTESIAN_POINT('Ctrl Pts',(-24.3949020994769,26.6672116108374,-26.7020392121718));
#29382=CARTESIAN_POINT('Ctrl Pts',(-24.1932089191864,26.7149803551183,-26.713625383618));
#29383=CARTESIAN_POINT('Ctrl Pts',(-23.820618542259,26.7660986835303,-26.7346507693911));
#29384=CARTESIAN_POINT('Ctrl Pts',(-23.65138925435,26.7758581450546,-26.7440662802989));
#29385=CARTESIAN_POINT('Ctrl Pts',(-23.3723933857431,26.7699642270149,-26.760150770649));
#29386=CARTESIAN_POINT('Ctrl Pts',(-23.2628019955691,26.7620348366198,-26.7666084160437));
#29387=CARTESIAN_POINT('Ctrl Pts',(-23.1327263931029,26.7459123981048,-26.7745324639313));
#29388=CARTESIAN_POINT('Ctrl Pts',(-23.1116428156245,26.7430869372719,-26.775824918877));
#29389=CARTESIAN_POINT('Ctrl Pts',(-23.0861361291948,26.7394113186635,-26.7773987524319));
#29390=CARTESIAN_POINT('Ctrl Pts',(-23.081684485776,26.7387603001642,-26.7776738094763));
#29391=CARTESIAN_POINT('Ctrl Pts',(-23.0730819547546,26.7374838417917,-26.7782060779828));
#29392=CARTESIAN_POINT('Ctrl Pts',(-23.0689308950522,26.7368596090413,-26.7784632507013));
#29393=CARTESIAN_POINT('Ctrl Pts',(-23.061779539548,26.7357699020578,-26.7789068791562));
#29394=CARTESIAN_POINT('Ctrl Pts',(-23.0587786528486,26.7353082937263,-26.7790932118733));
#29395=CARTESIAN_POINT('Ctrl Pts',(-23.0525865793213,26.7343468449782,-26.7794780569912));
#29396=CARTESIAN_POINT('Ctrl Pts',(-23.0493954835156,26.7338464463134,-26.7796765869559));
#29397=CARTESIAN_POINT('Ctrl Pts',(-23.0416930972526,26.7326267606781,-26.7801562650638));
#29398=CARTESIAN_POINT('Ctrl Pts',(-23.0371825823272,26.7319026787693,-26.7804375654599));
#29399=CARTESIAN_POINT('Ctrl Pts',(-23.0205596711014,26.7291979023252,-26.7814757506057));
#29400=CARTESIAN_POINT('Ctrl Pts',(-23.0084571978714,26.7271576303038,-26.7822345291494));
#29401=CARTESIAN_POINT('Ctrl Pts',(-22.8131164048176,26.6930778076623,-26.7945296334222));
#29402=CARTESIAN_POINT('Ctrl Pts',(-22.6330120593938,26.6453079987484,-26.8065804500814));
#29403=CARTESIAN_POINT('Ctrl Pts',(-22.4105157107109,26.5651606632149,-26.8223531931913));
#29404=CARTESIAN_POINT('Ctrl Pts',(-22.3633844825301,26.5469198563805,-26.8257450715511));
#29405=CARTESIAN_POINT('Ctrl Pts',(-22.2346156750902,26.4935690587107,-26.8351384017386));
#29406=CARTESIAN_POINT('Ctrl Pts',(-22.153992098097,26.4561880039129,-26.8411635288059));
#29407=CARTESIAN_POINT('Ctrl Pts',(-22.0750359193537,26.4155367251338,-26.8471666088699));
#29408=CARTESIAN_POINT('',(-26.7730021969517,23.548783660454,-26.6857734492732));
#29409=CARTESIAN_POINT('Ctrl Pts',(-22.075036065511,26.4155368003841,-27.0910469152906));
#29410=CARTESIAN_POINT('Ctrl Pts',(-22.1117303554584,26.4344291739391,-27.0882869220563));
#29411=CARTESIAN_POINT('Ctrl Pts',(-22.148792243511,26.4526190695116,-27.085542761816));
#29412=CARTESIAN_POINT('Ctrl Pts',(-22.2594218474688,26.5043014372093,-27.0774983103592));
#29413=CARTESIAN_POINT('Ctrl Pts',(-22.3339104340851,26.5357446747267,-27.0722699745989));
#29414=CARTESIAN_POINT('Ctrl Pts',(-22.4153638470589,26.5665722126063,-27.0668111573741));
#29415=CARTESIAN_POINT('Ctrl Pts',(-22.4212246077583,26.5687708259081,-27.0664198027816));
#29416=CARTESIAN_POINT('Ctrl Pts',(-22.4293900709342,26.5718069195685,-27.0658765620758));
#29417=CARTESIAN_POINT('Ctrl Pts',(-22.4316893305083,26.5726588478394,-27.0657238159769));
#29418=CARTESIAN_POINT('Ctrl Pts',(-22.4356529918019,26.5741223325226,-27.065460883452));
#29419=CARTESIAN_POINT('Ctrl Pts',(-22.4373169255687,26.5747351392394,-27.0653506217124));
#29420=CARTESIAN_POINT('Ctrl Pts',(-22.4407290852288,26.5759885993234,-27.0651247527524));
#29421=CARTESIAN_POINT('Ctrl Pts',(-22.4424773575766,26.5766291098535,-27.0650091546586));
#29422=CARTESIAN_POINT('Ctrl Pts',(-22.4465774975758,26.5781272398572,-27.0647383491723));
#29423=CARTESIAN_POINT('Ctrl Pts',(-22.4489298174668,26.5789836370416,-27.0645832155842));
#29424=CARTESIAN_POINT('Ctrl Pts',(-22.453903179367,26.5807877035772,-27.0642557119632));
#29425=CARTESIAN_POINT('Ctrl Pts',(-22.4565244598306,26.5817347162575,-27.0640833812348));
#29426=CARTESIAN_POINT('Ctrl Pts',(-22.4635801570312,26.5842734462758,-27.0636202759859));
#29427=CARTESIAN_POINT('Ctrl Pts',(-22.4680168622465,26.5858588494513,-27.0633298737699));
#29428=CARTESIAN_POINT('Ctrl Pts',(-22.481662201955,26.5907011293495,-27.0624391472207));
#29429=CARTESIAN_POINT('Ctrl Pts',(-22.4908822818475,26.5939259121944,-27.0618406728729));
#29430=CARTESIAN_POINT('Ctrl Pts',(-22.5249495504638,26.6056676045646,-27.0596413416516));
#29431=CARTESIAN_POINT('Ctrl Pts',(-22.5498866831905,26.6139228368537,-27.0580548651704));
#29432=CARTESIAN_POINT('Ctrl Pts',(-22.6375646623112,26.6417631738311,-27.0525494658113));
#29433=CARTESIAN_POINT('Ctrl Pts',(-22.7008045695414,26.6597342420235,-27.0487076966726));
#29434=CARTESIAN_POINT('Ctrl Pts',(-23.1479267347048,26.7721330564597,-27.022162150229));
#29435=CARTESIAN_POINT('Ctrl Pts',(-23.545741737267,26.7971594833623,-27.0012211057315));
#29436=CARTESIAN_POINT('Ctrl Pts',(-23.9568305774995,26.7473079199282,-26.9761541515665));
#29437=CARTESIAN_POINT('Ctrl Pts',(-23.9754169173656,26.7448893005317,-26.975014559856));
#29438=CARTESIAN_POINT('Ctrl Pts',(-23.9999718579269,26.7414759141054,-26.9735004027993));
#29439=CARTESIAN_POINT('Ctrl Pts',(-24.0059605246826,26.7406262360074,-26.9731304388732));
#29440=CARTESIAN_POINT('Ctrl Pts',(-24.0152529528623,26.7392811190478,-26.9725553120215));
#29441=CARTESIAN_POINT('Ctrl Pts',(-24.0185584178081,26.7387973909586,-26.9723505208016));
#29442=CARTESIAN_POINT('Ctrl Pts',(-24.0251741908387,26.7378187166248,-26.9719402165293));
#29443=CARTESIAN_POINT('Ctrl Pts',(-24.0284844919059,26.7373237511269,-26.9717347030976));
#29444=CARTESIAN_POINT('Ctrl Pts',(-24.0358721948227,26.7362073519493,-26.9712755773411));
#29445=CARTESIAN_POINT('Ctrl Pts',(-24.0399491815204,26.7355832468351,-26.97102188047));
#29446=CARTESIAN_POINT('Ctrl Pts',(-24.0518660012482,26.7337356005694,-26.9702793863383));
#29447=CARTESIAN_POINT('Ctrl Pts',(-24.0597024852284,26.7324909366055,-26.9697899184823));
#29448=CARTESIAN_POINT('Ctrl Pts',(-24.116989443313,26.7231750538389,-26.9662028460948));
#29449=CARTESIAN_POINT('Ctrl Pts',(-24.1662479564414,26.7139809078823,-26.9630696557072));
#29450=CARTESIAN_POINT('Ctrl Pts',(-24.3260858397578,26.680272746659,-26.9527351699353));
#29451=CARTESIAN_POINT('Ctrl Pts',(-24.4355809342886,26.6510802658873,-26.945388088509));
#29452=CARTESIAN_POINT('Ctrl Pts',(-24.6742678469254,26.5737700654847,-26.9287949825337));
#29453=CARTESIAN_POINT('Ctrl Pts',(-24.8023721830723,26.5230055533087,-26.9194953408774));
#29454=CARTESIAN_POINT('Ctrl Pts',(-24.9889587135771,26.434860562369,-26.9055264108721));
#29455=CARTESIAN_POINT('Ctrl Pts',(-25.0501337969723,26.4035305480273,-26.9008757124831));
#29456=CARTESIAN_POINT('Ctrl Pts',(-25.207388667933,26.3165384928552,-26.8887966559881));
#29457=CARTESIAN_POINT('Ctrl Pts',(-25.301685132614,26.2578209571642,-26.8814262590562));
#29458=CARTESIAN_POINT('Ctrl Pts',(-25.420215464717,26.1752239871941,-26.8721611929508));
#29459=CARTESIAN_POINT('Ctrl Pts',(-25.4473619559212,26.1556723758847,-26.8700394180871));
#29460=CARTESIAN_POINT('Ctrl Pts',(-25.4782575644331,26.1326815688672,-26.8676294277858));
#29461=CARTESIAN_POINT('Ctrl Pts',(-25.4823076611297,26.1296528720743,-26.8673135998061));
#29462=CARTESIAN_POINT('Ctrl Pts',(-25.4882690212393,26.1251729978878,-26.8668488949387));
#29463=CARTESIAN_POINT('Ctrl Pts',(-25.4901857947329,26.1237292182056,-26.8666995021319));
#29464=CARTESIAN_POINT('Ctrl Pts',(-25.4935544277947,26.1211859458161,-26.8664369986447));
#29465=CARTESIAN_POINT('Ctrl Pts',(-25.4950069681579,26.1200873631877,-26.8663238236793));
#29466=CARTESIAN_POINT('Ctrl Pts',(-25.4978515093721,26.1179321921358,-26.8661022217772));
#29467=CARTESIAN_POINT('Ctrl Pts',(-25.4992435774488,26.1168757062371,-26.8659937881466));
#29468=CARTESIAN_POINT('Ctrl Pts',(-25.5030079675217,26.114013959205,-26.8657006020191));
#29469=CARTESIAN_POINT('Ctrl Pts',(-25.5053786526177,26.112206532218,-26.8655160031056));
#29470=CARTESIAN_POINT('Ctrl Pts',(-25.5144524502014,26.1052686755528,-26.864809588611));
#29471=CARTESIAN_POINT('Ctrl Pts',(-25.5211379817682,26.1001151479354,-26.8642893945366));
#29472=CARTESIAN_POINT('Ctrl Pts',(-25.5377733974908,26.0871872582246,-26.8629955173038));
#29473=CARTESIAN_POINT('Ctrl Pts',(-25.5476980835186,26.0793804996065,-26.8622240460002));
#29474=CARTESIAN_POINT('Ctrl Pts',(-25.5867509088847,26.0482882705484,-26.859189032477));
#29475=CARTESIAN_POINT('Ctrl Pts',(-25.6155210571724,26.0245553377063,-26.8569546066483));
#29476=CARTESIAN_POINT('Ctrl Pts',(-25.6894226469634,25.961405442039,-26.8511995436364));
#29477=CARTESIAN_POINT('Ctrl Pts',(-25.7338795117567,25.9212188201317,-26.8477218094315));
#29478=CARTESIAN_POINT('Ctrl Pts',(-26.0545500009983,25.6146744723364,-26.8222951215269));
#29479=CARTESIAN_POINT('Ctrl Pts',(-26.2823220011113,25.302157492601,-26.8018640436458));
#29480=CARTESIAN_POINT('Ctrl Pts',(-26.4584747066371,24.9390487663431,-26.7774497082871));
#29481=CARTESIAN_POINT('Ctrl Pts',(-26.466969304452,24.9211188418543,-26.7762438771411));
#29482=CARTESIAN_POINT('Ctrl Pts',(-26.4778949051428,24.8974963759323,-26.7746544548105));
#29483=CARTESIAN_POINT('Ctrl Pts',(-26.4804759586782,24.8918733834103,-26.7742760601043));
#29484=CARTESIAN_POINT('Ctrl Pts',(-26.4844372364744,24.8831775213704,-26.7736907813634));
#29485=CARTESIAN_POINT('Ctrl Pts',(-26.4858288717208,24.880109840434,-26.7734842910414));
#29486=CARTESIAN_POINT('Ctrl Pts',(-26.4885924524867,24.873992406304,-26.7730724773471));
#29487=CARTESIAN_POINT('Ctrl Pts',(-26.4899644658967,24.8709426882141,-26.7728671566262));
#29488=CARTESIAN_POINT('Ctrl Pts',(-26.4929981009611,24.8641713604134,-26.7724112341954));
#29489=CARTESIAN_POINT('Ctrl Pts',(-26.4946574124827,24.860448727555,-26.7721605534873));
#29490=CARTESIAN_POINT('Ctrl Pts',(-26.4994326782185,24.8496806265695,-26.77143533832));
#29491=CARTESIAN_POINT('Ctrl Pts',(-26.502530421322,24.8426271566261,-26.7709601801534));
#29492=CARTESIAN_POINT('Ctrl Pts',(-26.5234532658806,24.7945186638534,-26.7677184542764));
#29493=CARTESIAN_POINT('Ctrl Pts',(-26.5404459694104,24.7531090038476,-26.7649236151799));
#29494=CARTESIAN_POINT('Ctrl Pts',(-26.5727237170193,24.6695361042963,-26.7592705182487));
#29495=CARTESIAN_POINT('Ctrl Pts',(-26.588002015373,24.6273809067697,-26.7564127809705));
#29496=CARTESIAN_POINT('Ctrl Pts',(-26.7155422445852,24.2511536329094,-26.7308484582895));
#29497=CARTESIAN_POINT('Ctrl Pts',(-26.7731442464588,23.9012054539653,-26.7062883839866));
#29498=CARTESIAN_POINT('Ctrl Pts',(-26.7730022699222,23.5489535893969,-26.6831828372533));
#29499=CARTESIAN_POINT('Ctrl Pts',(-26.7730021969517,23.548783660454,-26.6857734492732));
#29500=CARTESIAN_POINT('Ctrl Pts',(-26.772964759865,23.4666455156343,-26.6806758114827));
#29501=CARTESIAN_POINT('Ctrl Pts',(-26.7697874348417,23.3845817953304,-26.6755781736922));
#29502=CARTESIAN_POINT('Ctrl Pts',(-26.7634854691912,23.3027618209907,-26.6704805359017));
#29503=CARTESIAN_POINT('Ctrl Pts',(-26.7558552080702,23.2036962589499,-26.6643084445893));
#29504=CARTESIAN_POINT('Ctrl Pts',(-26.7436258552823,23.1048094192993,-26.658136353277));
#29505=CARTESIAN_POINT('Ctrl Pts',(-26.7268102442853,23.0065626742592,-26.6519642619647));
#29506=CARTESIAN_POINT('Ctrl Pts',(-26.7100174167789,22.9084490438458,-26.6458005332259));
#29507=CARTESIAN_POINT('Ctrl Pts',(-26.6886507545427,22.8109742086628,-26.6396368044871));
#29508=CARTESIAN_POINT('Ctrl Pts',(-26.6627749830657,22.7145961715745,-26.6334730757483));
#29509=CARTESIAN_POINT('Ctrl Pts',(-26.6369266245401,22.6183202379713,-26.6273158769017));
#29510=CARTESIAN_POINT('Ctrl Pts',(-26.6065787658576,22.5231392096193,-26.621158678055));
#29511=CARTESIAN_POINT('Ctrl Pts',(-26.5718473181805,22.4295016634016,-26.6150014792083));
#29512=CARTESIAN_POINT('Ctrl Pts',(-26.5371412570854,22.3359325605517,-26.6088487809006));
#29513=CARTESIAN_POINT('Ctrl Pts',(-26.4980581279732,22.2439051028591,-26.6026960825929));
#29514=CARTESIAN_POINT('Ctrl Pts',(-26.4547636208086,22.1538525547136,-26.5965433842852));
#29515=CARTESIAN_POINT('Ctrl Pts',(-26.4114855309827,22.0638341546225,-26.5903930190894));
#29516=CARTESIAN_POINT('Ctrl Pts',(-26.3639994242631,21.9757895671151,-26.5842426538937));
#29517=CARTESIAN_POINT('Ctrl Pts',(-26.3125186966516,21.890131091428,-26.5780922886979));
#29518=CARTESIAN_POINT('Ctrl Pts',(-26.2610437179955,21.8044821813936,-26.5719426103257));
#29519=CARTESIAN_POINT('Ctrl Pts',(-26.2055752291014,21.7212192257498,-26.5657929319535));
#29520=CARTESIAN_POINT('Ctrl Pts',(-26.1463715498038,21.6407280866269,-26.5596432535813));
#29521=CARTESIAN_POINT('Ctrl Pts',(-26.0871586432963,21.5602244025297,-26.5534926167488));
#29522=CARTESIAN_POINT('Ctrl Pts',(-26.0242096475015,21.4824937429909,-26.5473419799164));
#29523=CARTESIAN_POINT('Ctrl Pts',(-25.9578243828091,21.4078904371315,-26.5411913430839));
#29524=CARTESIAN_POINT('Ctrl Pts',(-25.8913680998289,21.3332073214065,-26.5350341263621));
#29525=CARTESIAN_POINT('Ctrl Pts',(-25.8214684965082,21.2616585653733,-26.5288769096403));
#29526=CARTESIAN_POINT('Ctrl Pts',(-25.74846354577,21.1935629254678,-26.5227196929184));
#29527=CARTESIAN_POINT('Ctrl Pts',(-25.6754178658689,21.1254292952837,-26.5165590411106));
#29528=CARTESIAN_POINT('Ctrl Pts',(-25.5992637194991,21.060752898994,-26.5103983893028));
#29529=CARTESIAN_POINT('Ctrl Pts',(-25.5203719548123,20.9998119773678,-26.504237737495));
#29530=CARTESIAN_POINT('Ctrl Pts',(-25.4413481761488,20.9387690799088,-26.498066776726));
#29531=CARTESIAN_POINT('Ctrl Pts',(-25.3595779846455,20.8814743922859,-26.491895815957));
#29532=CARTESIAN_POINT('Ctrl Pts',(-25.2754610805144,20.8281627048189,-26.4857248551879));
#29533=CARTESIAN_POINT('Ctrl Pts',(-25.2112530682199,20.7874688928001,-26.4810144449675));
#29534=CARTESIAN_POINT('Ctrl Pts',(-25.1456783284721,20.7490948998627,-26.4763040347471));
#29535=CARTESIAN_POINT('Ctrl Pts',(-25.0789230656487,20.7131265279504,-26.4715936245267));
#29536=CARTESIAN_POINT('Ctrl Pts',(-24.9914530665518,20.6659968586837,-26.4654215332144));
#29537=CARTESIAN_POINT('Ctrl Pts',(-24.901647425585,20.6228330894294,-26.4592494419021));
#29538=CARTESIAN_POINT('Ctrl Pts',(-24.8099012399664,20.5838738144283,-26.4530773505898));
#29539=CARTESIAN_POINT('Ctrl Pts',(-24.7182793613591,20.5449673253932,-26.446913621851));
#29540=CARTESIAN_POINT('Ctrl Pts',(-24.6247225603269,20.5102541761597,-26.4407498931122));
#29541=CARTESIAN_POINT('Ctrl Pts',(-24.5296511492348,20.4799274820521,-26.4345861643734));
#29542=CARTESIAN_POINT('Ctrl Pts',(-24.43468045738,20.4496329162307,-26.4284289655267));
#29543=CARTESIAN_POINT('Ctrl Pts',(-24.3381987571015,20.4237156980897,-26.42227176668));
#29544=CARTESIAN_POINT('Ctrl Pts',(-24.2406460985544,20.4023207844452,-26.4161145678333));
#29545=CARTESIAN_POINT('Ctrl Pts',(-24.143164745085,20.3809415091852,-26.4099618695256));
#29546=CARTESIAN_POINT('Ctrl Pts',(-24.0446144127321,20.36407805925,-26.4038091712179));
#29547=CARTESIAN_POINT('Ctrl Pts',(-23.9454491765465,20.3518252346625,-26.3976564729102));
#29548=CARTESIAN_POINT('Ctrl Pts',(-23.8463215439594,20.3395770563635,-26.3915061077145));
#29549=CARTESIAN_POINT('Ctrl Pts',(-23.7465799014946,20.3319360826576,-26.3853557425187));
#29550=CARTESIAN_POINT('Ctrl Pts',(-23.646686473003,20.3289456451241,-26.3792053773229));
#29551=CARTESIAN_POINT('Ctrl Pts',(-23.5468041998097,20.3259555415388,-26.3730556989507));
#29552=CARTESIAN_POINT('Ctrl Pts',(-23.4467706084967,20.3276149546168,-26.3669060205785));
#29553=CARTESIAN_POINT('Ctrl Pts',(-23.34704996417,20.3339151303864,-26.3607563422063));
#29554=CARTESIAN_POINT('Ctrl Pts',(-23.2473137778478,20.340216288072,-26.3546057053739));
#29555=CARTESIAN_POINT('Ctrl Pts',(-23.1478910689693,20.3511596176907,-26.3484550685414));
#29556=CARTESIAN_POINT('Ctrl Pts',(-23.0492420061998,20.3666844052292,-26.342304431709));
#29557=CARTESIAN_POINT('Ctrl Pts',(-22.9504874096561,20.3822258010291,-26.3361472149872));
#29558=CARTESIAN_POINT('Ctrl Pts',(-22.8525085418933,20.4023583742926,-26.3299899982653));
#29559=CARTESIAN_POINT('Ctrl Pts',(-22.7557562667419,20.4269700840957,-26.3238327815435));
#29560=CARTESIAN_POINT('Ctrl Pts',(-22.6589500138924,20.4515955246709,-26.3176721297357));
#29561=CARTESIAN_POINT('Ctrl Pts',(-22.563372132021,20.4807049517233,-26.3115114779279));
#29562=CARTESIAN_POINT('Ctrl Pts',(-22.4694571689025,20.5141367654119,-26.3053508261201));
#29563=CARTESIAN_POINT('Ctrl Pts',(-22.3753850526541,20.5476245224133,-26.2991798653511));
#29564=CARTESIAN_POINT('Ctrl Pts',(-22.2829818156605,20.5854489489311,-26.293008904582));
#29565=CARTESIAN_POINT('Ctrl Pts',(-22.1926610458664,20.6274006845922,-26.286837943813));
#29566=CARTESIAN_POINT('Ctrl Pts',(-22.1237175064283,20.659423232104,-26.2821275335926));
#29567=CARTESIAN_POINT('Ctrl Pts',(-22.0559868955778,20.6938495909111,-26.2774171233723));
#29568=CARTESIAN_POINT('Ctrl Pts',(-21.9896420512896,20.7305694837345,-26.2727067131519));
#29569=CARTESIAN_POINT('Ctrl Pts',(-21.9027098271538,20.7786838773609,-26.2665346218396));
#29570=CARTESIAN_POINT('Ctrl Pts',(-21.8178516677939,20.8309070227635,-26.2603625305272));
#29571=CARTESIAN_POINT('Ctrl Pts',(-21.7354818733435,20.8870354883256,-26.2541904392149));
#29572=CARTESIAN_POINT('Ctrl Pts',(-21.6532236818211,20.9430879053658,-26.2480267104761));
#29573=CARTESIAN_POINT('Ctrl Pts',(-21.573447509833,21.0030348830378,-26.2418629817373));
#29574=CARTESIAN_POINT('Ctrl Pts',(-21.4965430251931,21.0666271925162,-26.2356992529985));
#29575=CARTESIAN_POINT('Ctrl Pts',(-21.4197200136369,21.1301521319111,-26.2295420541518));
#29576=CARTESIAN_POINT('Ctrl Pts',(-21.3457629740193,21.1973144500351,-26.2233848553052));
#29577=CARTESIAN_POINT('Ctrl Pts',(-21.2750317267056,21.2678222806137,-26.2172276564585));
#29578=CARTESIAN_POINT('Ctrl Pts',(-21.2043521796445,21.3382785742439,-26.2110749581508));
#29579=CARTESIAN_POINT('Ctrl Pts',(-21.1368940437931,21.4120752127719,-26.2049222598431));
#29580=CARTESIAN_POINT('Ctrl Pts',(-21.0729825228156,21.48888141867,-26.1987695615354));
#29581=CARTESIAN_POINT('Ctrl Pts',(-21.0090952371777,21.5656584995456,-26.1926191963396));
#29582=CARTESIAN_POINT('Ctrl Pts',(-20.9487521716963,21.6454425466293,-26.1864688311439));
#29583=CARTESIAN_POINT('Ctrl Pts',(-20.8922396335423,21.7278681057955,-26.1803184659481));
#29584=CARTESIAN_POINT('Ctrl Pts',(-20.8357334062562,21.8102844603352,-26.1741687875759));
#29585=CARTESIAN_POINT('Ctrl Pts',(-20.783057101491,21.8953413822114,-26.1680191092037));
#29586=CARTESIAN_POINT('Ctrl Pts',(-20.734454309355,21.982643545508,-26.1618694308314));
#29587=CARTESIAN_POINT('Ctrl Pts',(-20.6858439422141,22.0699593153134,-26.155718793999));
#29588=CARTESIAN_POINT('Ctrl Pts',(-20.6413085600557,22.1595206420112,-26.1495681571665));
#29589=CARTESIAN_POINT('Ctrl Pts',(-20.601045823833,22.2509075594846,-26.1434175203341));
#29590=CARTESIAN_POINT('Ctrl Pts',(-20.5607400149404,22.3423922417623,-26.1372603036123));
#29591=CARTESIAN_POINT('Ctrl Pts',(-20.5247161549714,22.4357060164541,-26.1311030868904));
#29592=CARTESIAN_POINT('Ctrl Pts',(-20.4931236930307,22.5304090013857,-26.1249458701686));
#29593=CARTESIAN_POINT('Ctrl Pts',(-20.4615136057849,22.6251648207246,-26.1187852183608));
#29594=CARTESIAN_POINT('Ctrl Pts',(-20.4343399581838,22.7213109757304,-26.112624566553));
#29595=CARTESIAN_POINT('Ctrl Pts',(-20.4117016850638,22.8183945225043,-26.1064639147452));
#29596=CARTESIAN_POINT('Ctrl Pts',(-20.3890255300626,22.9156405245753,-26.1002929539761));
#29597=CARTESIAN_POINT('Ctrl Pts',(-20.3708999878733,23.0138266242466,-26.0941219932071));
#29598=CARTESIAN_POINT('Ctrl Pts',(-20.3573724819186,23.1124916948837,-26.0879510324381));
#29599=CARTESIAN_POINT('Ctrl Pts',(-20.3470466826322,23.1878045958268,-26.0832406222177));
#29600=CARTESIAN_POINT('Ctrl Pts',(-20.3393988894415,23.2633964015082,-26.0785302119973));
#29601=CARTESIAN_POINT('Ctrl Pts',(-20.3344297504739,23.3390620908957,-26.073819801777));
#29602=CARTESIAN_POINT('Ctrl Pts',(-20.327918644643,23.4382074991004,-26.0676477104646));
#29603=CARTESIAN_POINT('Ctrl Pts',(-20.3259854205563,23.5378289163274,-26.0614756191523));
#29604=CARTESIAN_POINT('Ctrl Pts',(-20.3286828745671,23.6374678215102,-26.05530352784));
#29605=CARTESIAN_POINT('Ctrl Pts',(-20.3313766737943,23.736971725827,-26.0491397991012));
#29606=CARTESIAN_POINT('Ctrl Pts',(-20.3386886690033,23.8364926405893,-26.0429760703624));
#29607=CARTESIAN_POINT('Ctrl Pts',(-20.3506198117746,23.9355680129816,-26.0368123416236));
#29608=CARTESIAN_POINT('Ctrl Pts',(-20.3625383146199,24.0345384243155,-26.0306551427769));
#29609=CARTESIAN_POINT('Ctrl Pts',(-20.3790661845488,24.1330638027741,-26.0244979439303));
#29610=CARTESIAN_POINT('Ctrl Pts',(-20.4001523677289,24.2306836593522,-26.0183407450836));
#29611=CARTESIAN_POINT('Ctrl Pts',(-20.4212231381879,24.328232161735,-26.0121880467759));
#29612=CARTESIAN_POINT('Ctrl Pts',(-20.4468455061786,24.424876034842,-26.0060353484682));
#29613=CARTESIAN_POINT('Ctrl Pts',(-20.4769169693841,24.5201628800977,-25.9998826501605));
#29614=CARTESIAN_POINT('Ctrl Pts',(-20.506977029448,24.6154135924462,-25.9937322849647));
#29615=CARTESIAN_POINT('Ctrl Pts',(-20.5414827018791,24.7093078856211,-25.987581919769));
#29616=CARTESIAN_POINT('Ctrl Pts',(-20.5802812851532,24.801407341148,-25.9814315545732));
#29617=CARTESIAN_POINT('Ctrl Pts',(-20.6190755357121,24.8934965117452,-25.975281876201));
#29618=CARTESIAN_POINT('Ctrl Pts',(-20.66216157536,24.9837908428531,-25.9691321978288));
#29619=CARTESIAN_POINT('Ctrl Pts',(-20.7093384805505,25.0718717076099,-25.9629825194566));
#29620=CARTESIAN_POINT('Ctrl Pts',(-20.7565227385139,25.1599663002403,-25.9568318826241));
#29621=CARTESIAN_POINT('Ctrl Pts',(-20.8077989233013,25.2458463583302,-25.9506812457917));
#29622=CARTESIAN_POINT('Ctrl Pts',(-20.8629205544969,25.3291185769132,-25.9445306089592));
#29623=CARTESIAN_POINT('Ctrl Pts',(-20.9181011542587,25.4124798792774,-25.9383733922374));
#29624=CARTESIAN_POINT('Ctrl Pts',(-20.9771351750754,25.493227408159,-25.9322161755156));
#29625=CARTESIAN_POINT('Ctrl Pts',(-21.0397333202698,25.5709976545559,-25.9260589587937));
#29626=CARTESIAN_POINT('Ctrl Pts',(-21.1023663887131,25.6488112886546,-25.9198983069859));
#29627=CARTESIAN_POINT('Ctrl Pts',(-21.1685672535822,25.723644007013,-25.9137376551781));
#29628=CARTESIAN_POINT('Ctrl Pts',(-21.2380083240489,25.7951677387144,-25.9075770033703));
#29629=CARTESIAN_POINT('Ctrl Pts',(-21.30756559412,25.8668111550531,-25.9014060426013));
#29630=CARTESIAN_POINT('Ctrl Pts',(-21.3803735832145,25.9351342270883,-25.8952350818323));
#29631=CARTESIAN_POINT('Ctrl Pts',(-21.4560699721281,25.9998477982044,-25.8890641210632));
#29632=CARTESIAN_POINT('Ctrl Pts',(-21.5138504470547,26.0492448820937,-25.8843537108428));
#29633=CARTESIAN_POINT('Ctrl Pts',(-21.5733131450406,26.0965396743571,-25.8796433006224));
#29634=CARTESIAN_POINT('Ctrl Pts',(-21.6342859287919,26.1416208071547,-25.874932890402));
#29635=CARTESIAN_POINT('Ctrl Pts',(-21.714165212207,26.2006807411426,-25.8687618716318));
#29636=CARTESIAN_POINT('Ctrl Pts',(-21.7969185090282,26.2561477796076,-25.8625908528617));
#29637=CARTESIAN_POINT('Ctrl Pts',(-21.8821887856859,26.3077298029972,-25.8564198340915));
#29638=CARTESIAN_POINT('Ctrl Pts',(-21.9451515000021,26.3458174500629,-25.8518632159228));
#29639=CARTESIAN_POINT('Ctrl Pts',(-22.0094857164726,26.3817876329866,-25.8473065977542));
#29640=CARTESIAN_POINT('Ctrl Pts',(-22.0750360153461,26.4155367745563,-25.8427499795855));
#29641=CARTESIAN_POINT('Origin',(-23.5502525316942,23.5502525316942,-77.3107734492734));
#29642=CARTESIAN_POINT('',(-22.0750358381979,26.41553668335,-24.3461133775544));
#29643=CARTESIAN_POINT('',(-22.0750360162151,26.4155367750037,-24.595751509546));
#29644=CARTESIAN_POINT('',(-22.0750360153461,26.4155367745563,-77.3107734492734));
#29645=CARTESIAN_POINT('Ctrl Pts',(-22.0750358381979,26.41553668335,-24.3461133775544));
#29646=CARTESIAN_POINT('Ctrl Pts',(-21.9942420567666,26.3739392958695,-24.3511965660311));
#29647=CARTESIAN_POINT('Ctrl Pts',(-21.915210609006,26.3289261847787,-24.3563001168851));
#29648=CARTESIAN_POINT('Ctrl Pts',(-21.7437655782969,26.2214199815303,-24.3678324034171));
#29649=CARTESIAN_POINT('Ctrl Pts',(-21.6525150813945,26.1573811521374,-24.3742908593729));
#29650=CARTESIAN_POINT('Ctrl Pts',(-21.5390546616165,26.068638211058,-24.3828717168821));
#29651=CARTESIAN_POINT('Ctrl Pts',(-21.513648116224,26.0481367645602,-24.3848309001178));
#29652=CARTESIAN_POINT('Ctrl Pts',(-21.478200653001,26.0186326016083,-24.3876205875967));
#29653=CARTESIAN_POINT('Ctrl Pts',(-21.4678975313913,26.0099469846117,-24.3884382972418));
#29654=CARTESIAN_POINT('Ctrl Pts',(-21.4500025419448,25.9946683393774,-24.3898707498562));
#29655=CARTESIAN_POINT('Ctrl Pts',(-21.442386442401,25.9881038820229,-24.3904843155895));
#29656=CARTESIAN_POINT('Ctrl Pts',(-21.4313292993113,25.9784829735044,-24.391380879353));
#29657=CARTESIAN_POINT('Ctrl Pts',(-21.4278638338603,25.9754545765195,-24.3916627094949));
#29658=CARTESIAN_POINT('Ctrl Pts',(-21.4218429421456,25.9701702577748,-24.3921538211899));
#29659=CARTESIAN_POINT('Ctrl Pts',(-21.4192845797578,25.9679176800463,-24.3923629627279));
#29660=CARTESIAN_POINT('Ctrl Pts',(-21.4143596290804,25.963567486651,-24.3927664613728));
#29661=CARTESIAN_POINT('Ctrl Pts',(-21.4119925438389,25.9614704371255,-24.392960794596));
#29662=CARTESIAN_POINT('Ctrl Pts',(-21.4064042304386,25.9565049349294,-24.3934205316858));
#29663=CARTESIAN_POINT('Ctrl Pts',(-21.4031856723078,25.9536334977325,-24.3936860610432));
#29664=CARTESIAN_POINT('Ctrl Pts',(-21.3936403042452,25.9450831190102,-24.3944757773306));
#29665=CARTESIAN_POINT('Ctrl Pts',(-21.3873302283899,25.9393856274369,-24.3950007477598));
#29666=CARTESIAN_POINT('Ctrl Pts',(-21.3298854188692,25.8871034771742,-24.3998068246709));
#29667=CARTESIAN_POINT('Ctrl Pts',(-21.2802438219251,25.8389119027674,-24.4041564342965));
#29668=CARTESIAN_POINT('Ctrl Pts',(-21.2082531198804,25.7643762605397,-24.4107750023431));
#29669=CARTESIAN_POINT('Ctrl Pts',(-21.1847121261474,25.7392074376824,-24.4129923546755));
#29670=CARTESIAN_POINT('Ctrl Pts',(-21.0736178722476,25.6165458569963,-24.4237153959014));
#29671=CARTESIAN_POINT('Ctrl Pts',(-20.9916693985912,25.514160270632,-24.4324258250087));
#29672=CARTESIAN_POINT('Ctrl Pts',(-20.835900403239,25.2931889296636,-24.4506278352556));
#29673=CARTESIAN_POINT('Ctrl Pts',(-20.7630866643506,25.1742109531433,-24.460115482091));
#29674=CARTESIAN_POINT('Ctrl Pts',(-20.6560132643234,24.9707122163578,-24.4755478720504));
#29675=CARTESIAN_POINT('Ctrl Pts',(-20.6172210949921,24.8887799985957,-24.4815622660975));
#29676=CARTESIAN_POINT('Ctrl Pts',(-20.5694664188923,24.7758365227026,-24.4894937801904));
#29677=CARTESIAN_POINT('Ctrl Pts',(-20.5574412069163,24.7461716431143,-24.4915443729831));
#29678=CARTESIAN_POINT('Ctrl Pts',(-20.5396624058426,24.7003646965779,-24.4946556751766));
#29679=CARTESIAN_POINT('Ctrl Pts',(-20.5335925928887,24.6843485339007,-24.4957333046094));
#29680=CARTESIAN_POINT('Ctrl Pts',(-20.5263193641045,24.6646853404913,-24.4970431785866));
#29681=CARTESIAN_POINT('Ctrl Pts',(-20.5249945541802,24.6610839578005,-24.4972825492739));
#29682=CARTESIAN_POINT('Ctrl Pts',(-20.5230545161551,24.6557809172264,-24.4976342236286));
#29683=CARTESIAN_POINT('Ctrl Pts',(-20.5224342900949,24.6540811109485,-24.4977468266259));
#29684=CARTESIAN_POINT('Ctrl Pts',(-20.5212364104313,24.6507895673814,-24.4979646388119));
#29685=CARTESIAN_POINT('Ctrl Pts',(-20.5206585796359,24.6491978968028,-24.4980698585799));
#29686=CARTESIAN_POINT('Ctrl Pts',(-20.519465785293,24.6459041804562,-24.4982873742448));
#29687=CARTESIAN_POINT('Ctrl Pts',(-20.518851002486,24.6442020763938,-24.4983996590513));
#29688=CARTESIAN_POINT('Ctrl Pts',(-20.5171802155366,24.6395640675289,-24.4987052919356));
#29689=CARTESIAN_POINT('Ctrl Pts',(-20.516127037101,24.6366271357791,-24.4988984699946));
#29690=CARTESIAN_POINT('Ctrl Pts',(-20.5121678759728,24.6255358086718,-24.4996266723458));
#29691=CARTESIAN_POINT('Ctrl Pts',(-20.5092904535769,24.6173711495599,-24.5001600029783));
#29692=CARTESIAN_POINT('Ctrl Pts',(-20.4609195629319,24.4783346514528,-24.5091975069974));
#29693=CARTESIAN_POINT('Ctrl Pts',(-20.4238729202963,24.3446553899401,-24.517217845754));
#29694=CARTESIAN_POINT('Ctrl Pts',(-20.3551706346225,24.0156382555668,-24.536272362119));
#29695=CARTESIAN_POINT('Ctrl Pts',(-20.3326574356841,23.8189847521018,-24.547117070942));
#29696=CARTESIAN_POINT('Ctrl Pts',(-20.3256208212519,23.5007927607372,-24.5651899284967));
#29697=CARTESIAN_POINT('Ctrl Pts',(-20.3297372762626,23.3800377929015,-24.5721640598763));
#29698=CARTESIAN_POINT('Ctrl Pts',(-20.3453062312673,23.2079899305531,-24.5824427175599));
#29699=CARTESIAN_POINT('Ctrl Pts',(-20.3512490558342,23.156297253546,-24.585574812308));
#29700=CARTESIAN_POINT('Ctrl Pts',(-20.3595523592231,23.0968049578778,-24.5892373976859));
#29701=CARTESIAN_POINT('Ctrl Pts',(-20.3606943141009,23.0888409285247,-24.5897288943518));
#29702=CARTESIAN_POINT('Ctrl Pts',(-20.3624701296571,23.0767780109904,-24.5904751976016));
#29703=CARTESIAN_POINT('Ctrl Pts',(-20.3630821067939,23.072675891899,-24.5907293094634));
#29704=CARTESIAN_POINT('Ctrl Pts',(-20.3641547980022,23.0655794749389,-24.5911694720465));
#29705=CARTESIAN_POINT('Ctrl Pts',(-20.3646118197373,23.0625846172243,-24.591355405287));
#29706=CARTESIAN_POINT('Ctrl Pts',(-20.365568049112,23.0563771639102,-24.5917411526894));
#29707=CARTESIAN_POINT('Ctrl Pts',(-20.3660678964055,23.0531646714878,-24.5919409869918));
#29708=CARTESIAN_POINT('Ctrl Pts',(-20.3672937210695,23.0453640785457,-24.5924267181702));
#29709=CARTESIAN_POINT('Ctrl Pts',(-20.3680247572274,23.0407767900571,-24.5927127756552));
#29710=CARTESIAN_POINT('Ctrl Pts',(-20.3708020896542,23.0235880918394,-24.5937862042517));
#29711=CARTESIAN_POINT('Ctrl Pts',(-20.3729133193837,23.0109974269687,-24.5945756389425));
#29712=CARTESIAN_POINT('Ctrl Pts',(-20.4083844396729,22.8069025392743,-24.607424484363));
#29713=CARTESIAN_POINT('Ctrl Pts',(-20.458921985018,22.6188262768828,-24.6200478186325));
#29714=CARTESIAN_POINT('Ctrl Pts',(-20.5918336647267,22.2579389643895,-24.6457555550066));
#29715=CARTESIAN_POINT('Ctrl Pts',(-20.6732649491656,22.0855835023762,-24.6587700828748));
#29716=CARTESIAN_POINT('Ctrl Pts',(-20.8033175417523,21.8635505196032,-24.6759683258234));
#29717=CARTESIAN_POINT('Ctrl Pts',(-20.8390145422813,21.8067488291666,-24.6804064953374));
#29718=CARTESIAN_POINT('Ctrl Pts',(-20.8974319489932,21.7199324189762,-24.6872057762782));
#29719=CARTESIAN_POINT('Ctrl Pts',(-20.9189481274954,21.6891329305297,-24.6896211211219));
#29720=CARTESIAN_POINT('Ctrl Pts',(-20.952303431785,21.6431214416742,-24.6932258971368));
#29721=CARTESIAN_POINT('Ctrl Pts',(-20.9637478094435,21.6276288332772,-24.6944390438673));
#29722=CARTESIAN_POINT('Ctrl Pts',(-20.9777246859083,21.6090585967343,-24.6958914920005));
#29723=CARTESIAN_POINT('Ctrl Pts',(-20.980124553005,21.6058823035649,-24.6961398615071));
#29724=CARTESIAN_POINT('Ctrl Pts',(-20.9836324166107,21.6012573871763,-24.6965014075827));
#29725=CARTESIAN_POINT('Ctrl Pts',(-20.9847357549222,21.5998052607723,-24.6966149112888));
#29726=CARTESIAN_POINT('Ctrl Pts',(-20.9868704247937,21.5970007227452,-24.6968340959611));
#29727=CARTESIAN_POINT('Ctrl Pts',(-20.9879015953884,21.5956481895299,-24.6969397883115));
#29728=CARTESIAN_POINT('Ctrl Pts',(-20.9900206387922,21.5928733084553,-24.6971566012376));
#29729=CARTESIAN_POINT('Ctrl Pts',(-20.9911086239971,21.5914510540718,-24.6972677132519));
#29730=CARTESIAN_POINT('Ctrl Pts',(-20.9937291751688,21.5880312829964,-24.6975348458409));
#29731=CARTESIAN_POINT('Ctrl Pts',(-20.9952629005193,21.5860346501976,-24.6976907839008));
#29732=CARTESIAN_POINT('Ctrl Pts',(-21.0008616586123,21.5787637335637,-24.6982585552015));
#29733=CARTESIAN_POINT('Ctrl Pts',(-21.0049407326039,21.573500207242,-24.6986693984758));
#29734=CARTESIAN_POINT('Ctrl Pts',(-21.0751090713098,21.483534191825,-24.7056893985408));
#29735=CARTESIAN_POINT('Ctrl Pts',(-21.1453851673489,21.4021653774305,-24.7120045047514));
#29736=CARTESIAN_POINT('Ctrl Pts',(-21.3948660591346,21.1409325738133,-24.7327511290629));
#29737=CARTESIAN_POINT('Ctrl Pts',(-21.5911937752434,20.9787518385778,-24.7465189818075));
#29738=CARTESIAN_POINT('Ctrl Pts',(-21.8797832001963,20.7927780074297,-24.7661495306448));
#29739=CARTESIAN_POINT('Ctrl Pts',(-21.9570250919267,20.7474400199854,-24.7713438428092));
#29740=CARTESIAN_POINT('Ctrl Pts',(-22.0893259150182,20.6770220488164,-24.7802253492873));
#29741=CARTESIAN_POINT('Ctrl Pts',(-22.1433850086716,20.6501692530227,-24.7838499385904));
#29742=CARTESIAN_POINT('Ctrl Pts',(-22.2057877483621,20.6213273781261,-24.7880404125832));
#29743=CARTESIAN_POINT('Ctrl Pts',(-22.2134256682169,20.61783338638,-24.788553416586));
#29744=CARTESIAN_POINT('Ctrl Pts',(-22.224921991625,20.6126286048934,-24.7893257556589));
#29745=CARTESIAN_POINT('Ctrl Pts',(-22.2287702815314,20.6108954526734,-24.7895843199667));
#29746=CARTESIAN_POINT('Ctrl Pts',(-22.2353957090791,20.6079272035765,-24.7900295357289));
#29747=CARTESIAN_POINT('Ctrl Pts',(-22.2381712165852,20.6066884636131,-24.7902160616375));
#29748=CARTESIAN_POINT('Ctrl Pts',(-22.2438918075935,20.6041449985452,-24.7906005470091));
#29749=CARTESIAN_POINT('Ctrl Pts',(-22.2468371025105,20.6028407591064,-24.7907985229131));
#29750=CARTESIAN_POINT('Ctrl Pts',(-22.253934027402,20.5997108073271,-24.791275613205));
#29751=CARTESIAN_POINT('Ctrl Pts',(-22.2580875575324,20.5978894424005,-24.7915548763077));
#29752=CARTESIAN_POINT('Ctrl Pts',(-22.2708518277206,20.5923242766125,-24.7924132218858));
#29753=CARTESIAN_POINT('Ctrl Pts',(-22.279475037692,20.5886093591834,-24.7929932909782));
#29754=CARTESIAN_POINT('Ctrl Pts',(-22.3806125536874,20.5455618927602,-24.7997991666576));
#29755=CARTESIAN_POINT('Ctrl Pts',(-22.4748928168715,20.5105450851924,-24.8061709491154));
#29756=CARTESIAN_POINT('Ctrl Pts',(-22.7967502871049,20.4078523582729,-24.8280470430414));
#29757=CARTESIAN_POINT('Ctrl Pts',(-23.0301059990025,20.3609168026128,-24.8441755224214));
#29758=CARTESIAN_POINT('Ctrl Pts',(-23.4347770175042,20.325142173986,-24.8716094853957));
#29759=CARTESIAN_POINT('Ctrl Pts',(-23.6040338753196,20.3235212395249,-24.8829017911953));
#29760=CARTESIAN_POINT('Ctrl Pts',(-23.7802520709472,20.3357112361222,-24.8939887584956));
#29761=CARTESIAN_POINT('Ctrl Pts',(-23.7878456990397,20.3362635742414,-24.8944651904783));
#29762=CARTESIAN_POINT('Ctrl Pts',(-23.7982875002998,20.337060289193,-24.8951184239805));
#29763=CARTESIAN_POINT('Ctrl Pts',(-23.8011373335486,20.3372815468779,-24.8952965137058));
#29764=CARTESIAN_POINT('Ctrl Pts',(-23.8059470911408,20.3376614090711,-24.8955967492564));
#29765=CARTESIAN_POINT('Ctrl Pts',(-23.807907164663,20.3378180157784,-24.8957190081312));
#29766=CARTESIAN_POINT('Ctrl Pts',(-23.8117693411559,20.3381301549741,-24.8959597246975));
#29767=CARTESIAN_POINT('Ctrl Pts',(-23.8136714494186,20.33828558316,-24.8960781880952));
#29768=CARTESIAN_POINT('Ctrl Pts',(-23.8178675274861,20.3386322123916,-24.8963393266138));
#29769=CARTESIAN_POINT('Ctrl Pts',(-23.8201614367503,20.3388241821308,-24.8964819580899));
#29770=CARTESIAN_POINT('Ctrl Pts',(-23.8281871675072,20.3395044891259,-24.8969805444856));
#29771=CARTESIAN_POINT('Ctrl Pts',(-23.8339179294859,20.3400057190726,-24.8973357735987));
#29772=CARTESIAN_POINT('Ctrl Pts',(-23.8924304317722,20.3452813076583,-24.9009550037664));
#29773=CARTESIAN_POINT('Ctrl Pts',(-23.9450918740019,20.3513419424527,-24.9041479392798));
#29774=CARTESIAN_POINT('Ctrl Pts',(-24.3053621488696,20.4018377480508,-24.9256953060309));
#29775=CARTESIAN_POINT('Ctrl Pts',(-24.6053151435294,20.4892720706137,-24.9422885620987));
#29776=CARTESIAN_POINT('Ctrl Pts',(-25.0082028413813,20.6731155715469,-24.9676174329098));
#29777=CARTESIAN_POINT('Ctrl Pts',(-25.1247799959606,20.7352226792367,-24.9753316666834));
#29778=CARTESIAN_POINT('Ctrl Pts',(-25.2551571926593,20.8153190460711,-24.984583487794));
#29779=CARTESIAN_POINT('Ctrl Pts',(-25.2729923736557,20.826518242533,-24.985863138569));
#29780=CARTESIAN_POINT('Ctrl Pts',(-25.2958604313623,20.8411921812023,-24.9875225668843));
#29781=CARTESIAN_POINT('Ctrl Pts',(-25.300995243951,20.8445077402075,-24.9878964028895));
#29782=CARTESIAN_POINT('Ctrl Pts',(-25.3092449414227,20.8498679020947,-24.9884990060819));
#29783=CARTESIAN_POINT('Ctrl Pts',(-25.3123657839856,20.8519033454001,-24.9887274299295));
#29784=CARTESIAN_POINT('Ctrl Pts',(-25.3182969246568,20.8557863696564,-24.9891624280565));
#29785=CARTESIAN_POINT('Ctrl Pts',(-25.3211078760074,20.8576329478625,-24.9893689644735));
#29786=CARTESIAN_POINT('Ctrl Pts',(-25.327501034483,20.861847101054,-24.9898395684709));
#29787=CARTESIAN_POINT('Ctrl Pts',(-25.3310814052966,20.8642174383234,-24.9901037398517));
#29788=CARTESIAN_POINT('Ctrl Pts',(-25.3419530551118,20.8714461624883,-24.9909077750359));
#29789=CARTESIAN_POINT('Ctrl Pts',(-25.349229223334,20.8763271045706,-24.9914484901306));
#29790=CARTESIAN_POINT('Ctrl Pts',(-25.4008117339563,20.9112351234727,-24.9953003538391));
#29791=CARTESIAN_POINT('Ctrl Pts',(-25.4443816440976,20.9423306404437,-24.9986520302611));
#29792=CARTESIAN_POINT('Ctrl Pts',(-25.4955332093108,20.9807952869625,-25.0027096482574));
#29793=CARTESIAN_POINT('Ctrl Pts',(-25.5038804688768,20.987136200711,-25.0033757999959));
#29794=CARTESIAN_POINT('Ctrl Pts',(-25.7604356513508,21.1840071851929,-25.0239743455247));
#29795=CARTESIAN_POINT('Ctrl Pts',(-25.9795760202373,21.4096135289019,-25.0454125857946));
#29796=CARTESIAN_POINT('Ctrl Pts',(-26.2145839418957,21.7349565496501,-25.0723390774719));
#29797=CARTESIAN_POINT('Ctrl Pts',(-26.2634661549541,21.8088635518611,-25.0782164990782));
#29798=CARTESIAN_POINT('Ctrl Pts',(-26.3340400323854,21.9257690607955,-25.0870527925547));
#29799=CARTESIAN_POINT('Ctrl Pts',(-26.35791678203,21.9673938916192,-25.0901133549678));
#29800=CARTESIAN_POINT('Ctrl Pts',(-26.3832419160754,22.0139213161168,-25.0934280746687));
#29801=CARTESIAN_POINT('Ctrl Pts',(-26.3856170279805,22.0183091156466,-25.0937396425749));
#29802=CARTESIAN_POINT('Ctrl Pts',(-26.3891253037819,22.024826438771,-25.0942008785615));
#29803=CARTESIAN_POINT('Ctrl Pts',(-26.3902662676191,22.026951720652,-25.0943510433309));
#29804=CARTESIAN_POINT('Ctrl Pts',(-26.3922078700308,22.0305781219144,-25.0946068549077));
#29805=CARTESIAN_POINT('Ctrl Pts',(-26.3930097061134,22.0320785943001,-25.0947125788137));
#29806=CARTESIAN_POINT('Ctrl Pts',(-26.3946525539107,22.0351587132599,-25.0949293551341));
#29807=CARTESIAN_POINT('Ctrl Pts',(-26.395493436236,22.0367384220128,-25.0950403991395));
#29808=CARTESIAN_POINT('Ctrl Pts',(-26.3975122473545,22.0405386540711,-25.0953072109253));
#29809=CARTESIAN_POINT('Ctrl Pts',(-26.3986888971739,22.0427598608585,-25.0954628966264));
#29810=CARTESIAN_POINT('Ctrl Pts',(-26.4029620255938,22.0508492737995,-25.0960289372831));
#29811=CARTESIAN_POINT('Ctrl Pts',(-26.4060430064908,22.0567257149562,-25.0964383099897));
#29812=CARTESIAN_POINT('Ctrl Pts',(-26.4577959584851,22.1561812384885,-25.1033367305253));
#29813=CARTESIAN_POINT('Ctrl Pts',(-26.501868974304,22.2520964265145,-25.1095423662194));
#29814=CARTESIAN_POINT('Ctrl Pts',(-26.6470901888889,22.6139767095907,-25.1319578696367));
#29815=CARTESIAN_POINT('Ctrl Pts',(-26.7176115374808,22.8908052075387,-25.1472952514175));
#29816=CARTESIAN_POINT('Ctrl Pts',(-26.763440811863,23.2799435771829,-25.1699287516284));
#29817=CARTESIAN_POINT('Ctrl Pts',(-26.7706612529901,23.3871273484865,-25.176256398643));
#29818=CARTESIAN_POINT('Ctrl Pts',(-26.7728416733939,23.5130652031083,-25.1838833289959));
#29819=CARTESIAN_POINT('Ctrl Pts',(-26.773002644352,23.5316686044944,-25.1850147830875));
#29820=CARTESIAN_POINT('Ctrl Pts',(-26.7730024965163,23.5560682488993,-25.1865053929689));
#29821=CARTESIAN_POINT('Ctrl Pts',(-26.772986824523,23.5618643988586,-25.1868599786412));
#29822=CARTESIAN_POINT('Ctrl Pts',(-26.7729377463209,23.5709501786123,-25.1874165900529));
#29823=CARTESIAN_POINT('Ctrl Pts',(-26.7729149391584,23.5742398731262,-25.18761828284));
#29824=CARTESIAN_POINT('Ctrl Pts',(-26.7728615327684,23.5805495615121,-25.1880054422562));
#29825=CARTESIAN_POINT('Ctrl Pts',(-26.7728317253419,23.5835695602356,-25.1881908838321));
#29826=CARTESIAN_POINT('Ctrl Pts',(-26.7727518242488,23.5906555902458,-25.1886263190768));
#29827=CARTESIAN_POINT('Ctrl Pts',(-26.7726982801883,23.5947215706633,-25.1888764208102));
#29828=CARTESIAN_POINT('Ctrl Pts',(-26.7725216750178,23.606446944656,-25.1895983790682));
#29829=CARTESIAN_POINT('Ctrl Pts',(-26.7723790003642,23.6141059758931,-25.1900708506798));
#29830=CARTESIAN_POINT('Ctrl Pts',(-26.7712362172908,23.6655939150874,-25.1932531001028));
#29831=CARTESIAN_POINT('Ctrl Pts',(-26.7693692134111,23.7093971855818,-25.1959899785362));
#29832=CARTESIAN_POINT('Ctrl Pts',(-26.7619186212252,23.8275066412046,-25.2034541201707));
#29833=CARTESIAN_POINT('Ctrl Pts',(-26.7546509317697,23.901675869812,-25.2082324795851));
#29834=CARTESIAN_POINT('Ctrl Pts',(-26.724906397274,24.1251128121717,-25.2229054033648));
#29835=CARTESIAN_POINT('Ctrl Pts',(-26.6945118729874,24.2731054473815,-25.2330126697525));
#29836=CARTESIAN_POINT('Ctrl Pts',(-26.590672507125,24.6443251435024,-25.2590688590711));
#29837=CARTESIAN_POINT('Ctrl Pts',(-26.5029950011948,24.8626862556386,-25.2751013124365));
#29838=CARTESIAN_POINT('Ctrl Pts',(-26.3861254169185,25.0813039438851,-25.2907489502845));
#29839=CARTESIAN_POINT('Ctrl Pts',(-26.3798007370111,25.0929613234707,-25.2915818772712));
#29840=CARTESIAN_POINT('Ctrl Pts',(-26.3716419636381,25.1077802474873,-25.2926385140698));
#29841=CARTESIAN_POINT('Ctrl Pts',(-26.3698743296894,25.1109779491634,-25.2928663900156));
#29842=CARTESIAN_POINT('Ctrl Pts',(-26.3670574117202,25.1160534313222,-25.2932278652182));
#29843=CARTESIAN_POINT('Ctrl Pts',(-26.3660116859845,25.1179331670627,-25.2933616926141));
#29844=CARTESIAN_POINT('Ctrl Pts',(-26.3640550236922,25.1214420754794,-25.2936114184695));
#29845=CARTESIAN_POINT('Ctrl Pts',(-26.3631445598176,25.1230714928659,-25.2937273460361));
#29846=CARTESIAN_POINT('Ctrl Pts',(-26.3610992378097,25.1267244597029,-25.2939871610301));
#29847=CARTESIAN_POINT('Ctrl Pts',(-26.3599636123488,25.1287475707767,-25.2941309977533));
#29848=CARTESIAN_POINT('Ctrl Pts',(-26.3566017512803,25.1347215865861,-25.2945555715205));
#29849=CARTESIAN_POINT('Ctrl Pts',(-26.3543693480444,25.1386690416312,-25.2948359109001));
#29850=CARTESIAN_POINT('Ctrl Pts',(-26.3369167534398,25.1693781964003,-25.2970152998891));
#29851=CARTESIAN_POINT('Ctrl Pts',(-26.3213214519027,25.19592643981,-25.2988904724722));
#29852=CARTESIAN_POINT('Ctrl Pts',(-26.2659851992392,25.2871088638027,-25.3053143200299));
#29853=CARTESIAN_POINT('Ctrl Pts',(-26.2243416399564,25.350564477048,-25.3097556288964));
#29854=CARTESIAN_POINT('Ctrl Pts',(-25.9947049575678,25.6749044566902,-25.3326233146511));
#29855=CARTESIAN_POINT('Ctrl Pts',(-25.7706983366996,25.9080351566661,-25.3498404506165));
#29856=CARTESIAN_POINT('Ctrl Pts',(-25.4996794513211,26.1166254322822,-25.3698751400516));
#29857=CARTESIAN_POINT('Ctrl Pts',(-25.4833670027122,26.1289350627727,-25.371077468022));
#29858=CARTESIAN_POINT('Ctrl Pts',(-25.463399221677,26.1437071179424,-25.3725455591721));
#29859=CARTESIAN_POINT('Ctrl Pts',(-25.4598542611247,26.146318436677,-25.3728060564054));
#29860=CARTESIAN_POINT('Ctrl Pts',(-25.4530687889067,26.1512953900363,-25.3733044229119));
#29861=CARTESIAN_POINT('Ctrl Pts',(-25.4498291872766,26.153662255308,-25.3735422480229));
#29862=CARTESIAN_POINT('Ctrl Pts',(-25.4426371394999,26.1588962215782,-25.3740699915606));
#29863=CARTESIAN_POINT('Ctrl Pts',(-25.4386825853658,26.161760398167,-25.3743600131102));
#29864=CARTESIAN_POINT('Ctrl Pts',(-25.4290878115077,26.1686764438218,-25.3750633118715));
#29865=CARTESIAN_POINT('Ctrl Pts',(-25.4234409908385,26.1727190782331,-25.3754769175077));
#29866=CARTESIAN_POINT('Ctrl Pts',(-25.4162456212369,26.1778352425375,-25.3760035799283));
#29867=CARTESIAN_POINT('Ctrl Pts',(-25.4147091087239,26.1789257302666,-25.3761160231406));
#29868=CARTESIAN_POINT('Ctrl Pts',(-25.4078589152983,26.183778395495,-25.3766172326296));
#29869=CARTESIAN_POINT('Ctrl Pts',(-25.4025348237314,26.1875257942529,-25.3770065321166));
#29870=CARTESIAN_POINT('Ctrl Pts',(-25.3933405446863,26.1939556755297,-25.3776784155976));
#29871=CARTESIAN_POINT('Ctrl Pts',(-25.38947575301,26.1966458656836,-25.3779607172545));
#29872=CARTESIAN_POINT('Ctrl Pts',(-25.3760585976065,26.2059416426025,-25.3789403582186));
#29873=CARTESIAN_POINT('Ctrl Pts',(-25.3664765136131,26.2125040010901,-25.3796392704975));
#29874=CARTESIAN_POINT('Ctrl Pts',(-25.3529516299144,26.2216596123777,-25.3806248661675));
#29875=CARTESIAN_POINT('Ctrl Pts',(-25.3490382096055,26.2242962699358,-25.3809099423132));
#29876=CARTESIAN_POINT('Ctrl Pts',(-25.3283307484909,26.2381818454686,-25.3824178597072));
#29877=CARTESIAN_POINT('Ctrl Pts',(-25.3114372345221,26.2492809780931,-25.383646198793));
#29878=CARTESIAN_POINT('Ctrl Pts',(-25.2891999355987,26.2635933382306,-25.3852611017637));
#29879=CARTESIAN_POINT('Ctrl Pts',(-25.2839494047233,26.2669511821796,-25.3856422586221));
#29880=CARTESIAN_POINT('Ctrl Pts',(-25.2758384527454,26.2721052462623,-25.3862308561582));
#29881=CARTESIAN_POINT('Ctrl Pts',(-25.2729848725658,26.2739122483821,-25.3864378957839));
#29882=CARTESIAN_POINT('Ctrl Pts',(-25.2673011265986,26.2774989199629,-25.386850199858));
#29883=CARTESIAN_POINT('Ctrl Pts',(-25.2644710215902,26.2792786782073,-25.3870554606738));
#29884=CARTESIAN_POINT('Ctrl Pts',(-25.2581976393072,26.2832101892727,-25.3875103737555));
#29885=CARTESIAN_POINT('Ctrl Pts',(-25.25475305876,26.285359842519,-25.3877601032832));
#29886=CARTESIAN_POINT('Ctrl Pts',(-25.2449515517711,26.2914509447047,-25.3884705590168));
#29887=CARTESIAN_POINT('Ctrl Pts',(-25.2385849843963,26.295376761266,-25.3889318610918));
#29888=CARTESIAN_POINT('Ctrl Pts',(-25.1975301416009,26.320495564185,-25.3919055275477));
#29889=CARTESIAN_POINT('Ctrl Pts',(-25.1624584995583,26.3410519971134,-25.394441117158));
#29890=CARTESIAN_POINT('Ctrl Pts',(-25.0569090985583,26.4002637512238,-25.4020624068653));
#29891=CARTESIAN_POINT('Ctrl Pts',(-24.9853683382631,26.4369493933388,-25.4072163515426));
#29892=CARTESIAN_POINT('Ctrl Pts',(-24.7745449265404,26.5352834901584,-25.4223735829986));
#29893=CARTESIAN_POINT('Ctrl Pts',(-24.6321792707311,26.589780091718,-25.4325812533794));
#29894=CARTESIAN_POINT('Ctrl Pts',(-24.2856361981713,26.6949938428261,-25.4570697029826));
#29895=CARTESIAN_POINT('Ctrl Pts',(-24.0792687220177,26.7362129017849,-25.4713853704981));
#29896=CARTESIAN_POINT('Ctrl Pts',(-23.864664158185,26.7576339377859,-25.4852012007488));
#29897=CARTESIAN_POINT('Ctrl Pts',(-23.8589818607033,26.7581858784842,-25.4855662287531));
#29898=CARTESIAN_POINT('Ctrl Pts',(-23.8491217673299,26.7591171813321,-25.4861982364657));
#29899=CARTESIAN_POINT('Ctrl Pts',(-23.8449446599103,26.759503489428,-25.4864655432152));
#29900=CARTESIAN_POINT('Ctrl Pts',(-23.8246727901913,26.761338364082,-25.487760655175));
#29901=CARTESIAN_POINT('Ctrl Pts',(-23.808567676587,26.7626740501463,-25.4887829877595));
#29902=CARTESIAN_POINT('Ctrl Pts',(-23.7834862285339,26.7645643494126,-25.4903641880516));
#29903=CARTESIAN_POINT('Ctrl Pts',(-23.7745167244039,26.7652026083401,-25.4909274743598));
#29904=CARTESIAN_POINT('Ctrl Pts',(-23.7623816169219,26.7660150948552,-25.4916865131141));
#29905=CARTESIAN_POINT('Ctrl Pts',(-23.7592183669247,26.7662221974934,-25.4918840912387));
#29906=CARTESIAN_POINT('Ctrl Pts',(-23.75423882804,26.7665408372821,-25.4921946694891));
#29907=CARTESIAN_POINT('Ctrl Pts',(-23.7524227522241,26.7666555032961,-25.4923078463569));
#29908=CARTESIAN_POINT('Ctrl Pts',(-23.7489196819735,26.7668737065528,-25.4925259744105));
#29909=CARTESIAN_POINT('Ctrl Pts',(-23.7472327145148,26.7669774541484,-25.4926309366481));
#29910=CARTESIAN_POINT('Ctrl Pts',(-23.7432148351371,26.7672213790242,-25.4928807343515));
#29911=CARTESIAN_POINT('Ctrl Pts',(-23.7408838538725,26.7673603499573,-25.4930255007715));
#29912=CARTESIAN_POINT('Ctrl Pts',(-23.7340450090293,26.7677606166555,-25.4934497825451));
#29913=CARTESIAN_POINT('Ctrl Pts',(-23.7295367212226,26.7680149734371,-25.4937289067766));
#29914=CARTESIAN_POINT('Ctrl Pts',(-23.6968968366111,26.7697877000548,-25.4957457301195));
#29915=CARTESIAN_POINT('Ctrl Pts',(-23.6687458053862,26.7709466692085,-25.497463526227));
#29916=CARTESIAN_POINT('Ctrl Pts',(-23.5753301375406,26.7735660187263,-25.5031026907515));
#29917=CARTESIAN_POINT('Ctrl Pts',(-23.510032919845,26.7734128327498,-25.5069456578207));
#29918=CARTESIAN_POINT('Ctrl Pts',(-23.1813916093272,26.7626515615342,-25.5259887504925));
#29919=CARTESIAN_POINT('Ctrl Pts',(-22.9200420020355,26.7217539591146,-25.5402446042775));
#29920=CARTESIAN_POINT('Ctrl Pts',(-22.5195078414425,26.6075503236672,-25.5640006145775));
#29921=CARTESIAN_POINT('Ctrl Pts',(-22.3756324402608,26.5552088110836,-25.5729361593038));
#29922=CARTESIAN_POINT('Ctrl Pts',(-22.2257724556061,26.4882784400287,-25.5829187877678));
#29923=CARTESIAN_POINT('Ctrl Pts',(-22.2155413559588,26.483644728855,-25.5836037374406));
#29924=CARTESIAN_POINT('Ctrl Pts',(-22.201337443255,26.4771220188907,-25.5845595067221));
#29925=CARTESIAN_POINT('Ctrl Pts',(-22.1973438769779,26.475278186724,-25.5848287660469));
#29926=CARTESIAN_POINT('Ctrl Pts',(-22.19046550888,26.4720853395405,-25.5852934573601));
#29927=CARTESIAN_POINT('Ctrl Pts',(-22.1875789009828,26.4707402102292,-25.5854887546627));
#29928=CARTESIAN_POINT('Ctrl Pts',(-22.1816192627898,26.4679523213986,-25.5858925487251));
#29929=CARTESIAN_POINT('Ctrl Pts',(-22.1785465104716,26.4665089811164,-25.5861010654169));
#29930=CARTESIAN_POINT('Ctrl Pts',(-22.1713894614715,26.4631333413704,-25.5865874983815));
#29931=CARTESIAN_POINT('Ctrl Pts',(-22.1673069440084,26.4611973059852,-25.5868655442008));
#29932=CARTESIAN_POINT('Ctrl Pts',(-22.1545432197083,26.4551115064115,-25.5877366467598));
#29933=CARTESIAN_POINT('Ctrl Pts',(-22.1458765779327,26.4509314735687,-25.5883307567479));
#29934=CARTESIAN_POINT('Ctrl Pts',(-22.1163850462825,26.4365441768311,-25.5903615011968));
#29935=CARTESIAN_POINT('Ctrl Pts',(-22.0956529123993,26.426151563364,-25.591804560725));
#29936=CARTESIAN_POINT('Ctrl Pts',(-22.0750360129136,26.4155367733039,-25.5932554334314));
#29937=CARTESIAN_POINT('',(-26.7730012125181,23.5531684787983,-25.4357734492732));
#29938=CARTESIAN_POINT('Ctrl Pts',(-22.0750360153461,26.4155367745563,-25.8427499795855));
#29939=CARTESIAN_POINT('Ctrl Pts',(-22.1636338262233,26.4611521281618,-25.8365912525975));
#29940=CARTESIAN_POINT('Ctrl Pts',(-22.2544540515615,26.5027082272478,-25.8304325256094));
#29941=CARTESIAN_POINT('Ctrl Pts',(-22.3470880535136,26.5399871020105,-25.8242737986213));
#29942=CARTESIAN_POINT('Ctrl Pts',(-22.4399842542781,26.5773714939319,-25.8180976394716));
#29943=CARTESIAN_POINT('Ctrl Pts',(-22.5347041380959,26.6104541829362,-25.8119214803219));
#29944=CARTESIAN_POINT('Ctrl Pts',(-22.6308118557336,26.6390624005416,-25.8057453211721));
#29945=CARTESIAN_POINT('Ctrl Pts',(-22.7265250860868,26.6675531918013,-25.7995945129131));
#29946=CARTESIAN_POINT('Ctrl Pts',(-22.8236143597423,26.6916060486344,-25.7934437046541));
#29947=CARTESIAN_POINT('Ctrl Pts',(-22.921631680785,26.7110994733069,-25.7872928963952));
#29948=CARTESIAN_POINT('Ctrl Pts',(-23.0196313073245,26.7305893789435,-25.7811431985062));
#29949=CARTESIAN_POINT('Ctrl Pts',(-23.118558222282,26.7455214036659,-25.7749935006173));
#29950=CARTESIAN_POINT('Ctrl Pts',(-23.2179534647942,26.7558250067191,-25.7688438027283));
#29951=CARTESIAN_POINT('Ctrl Pts',(-23.3173573550546,26.7661295062234,-25.7626935697933));
#29952=CARTESIAN_POINT('Ctrl Pts',(-23.4172292216113,26.7718047397265,-25.7565433368582));
#29953=CARTESIAN_POINT('Ctrl Pts',(-23.5171052057916,26.7728320601598,-25.7503931039231));
#29954=CARTESIAN_POINT('Ctrl Pts',(-23.6177178214486,26.7738669575554,-25.7441975101818));
#29955=CARTESIAN_POINT('Ctrl Pts',(-23.7183341686747,26.77018508424,-25.7380019164405));
#29956=CARTESIAN_POINT('Ctrl Pts',(-23.8184818372402,26.7618207782283,-25.7318063226992));
#29957=CARTESIAN_POINT('Ctrl Pts',(-23.9180485167876,26.7535049962613,-25.7256466716011));
#29958=CARTESIAN_POINT('Ctrl Pts',(-24.0171515152515,26.7405610834495,-25.719487020503));
#29959=CARTESIAN_POINT('Ctrl Pts',(-24.1153348872376,26.7230745396161,-25.713327369405));
#29960=CARTESIAN_POINT('Ctrl Pts',(-24.2143776349878,26.7054349402126,-25.707113804342));
#29961=CARTESIAN_POINT('Ctrl Pts',(-24.3124841403336,26.6831729071579,-25.700900239279));
#29962=CARTESIAN_POINT('Ctrl Pts',(-24.4092014443937,26.6564277244147,-25.6946866742161));
#29963=CARTESIAN_POINT('Ctrl Pts',(-24.5059187484537,26.6296825416715,-25.6884731091531));
#29964=CARTESIAN_POINT('Ctrl Pts',(-24.6012464461555,26.5984544082594,-25.6822595440902));
#29965=CARTESIAN_POINT('Ctrl Pts',(-24.6947529679961,26.5629317900629,-25.6760459790272));
#29966=CARTESIAN_POINT('Ctrl Pts',(-24.7876353608333,26.5276462750743,-25.6698738877149));
#29967=CARTESIAN_POINT('Ctrl Pts',(-24.8790480053133,26.4879991748671,-25.6637017964026));
#29968=CARTESIAN_POINT('Ctrl Pts',(-24.9685519169491,26.444133043444,-25.6575297050903));
#29969=CARTESIAN_POINT('Ctrl Pts',(-25.0579345596333,26.4003263462923,-25.6513659763515));
#29970=CARTESIAN_POINT('Ctrl Pts',(-25.1454132230758,26.3523121693096,-25.6452022476127));
#29971=CARTESIAN_POINT('Ctrl Pts',(-25.2305668039053,26.300281896829,-25.639038518874));
#29972=CARTESIAN_POINT('Ctrl Pts',(-25.315630172508,26.2483067455388,-25.6328813200273));
#29973=CARTESIAN_POINT('Ctrl Pts',(-25.3983729869398,26.1923241826761,-25.6267241211806));
#29974=CARTESIAN_POINT('Ctrl Pts',(-25.478397635834,26.1325720355282,-25.6205669223339));
#29975=CARTESIAN_POINT('Ctrl Pts',(-25.5583637915627,26.0728635635764,-25.6144142240262));
#29976=CARTESIAN_POINT('Ctrl Pts',(-25.6356153848488,26.0093912445286,-25.6082615257185));
#29977=CARTESIAN_POINT('Ctrl Pts',(-25.7097835462753,25.9424363372498,-25.6021088274108));
#29978=CARTESIAN_POINT('Ctrl Pts',(-25.7839235830294,25.875506819367,-25.5959584622151));
#29979=CARTESIAN_POINT('Ctrl Pts',(-25.8549821891059,25.805097628041,-25.5898080970194));
#29980=CARTESIAN_POINT('Ctrl Pts',(-25.9226240746639,25.7315298695419,-25.5836577318236));
#29981=CARTESIAN_POINT('Ctrl Pts',(-25.9902584065176,25.657970326501,-25.5775080534514));
#29982=CARTESIAN_POINT('Ctrl Pts',(-26.0544764824102,25.5812532373267,-25.5713583750792));
#29983=CARTESIAN_POINT('Ctrl Pts',(-26.1149810560759,25.5017353419498,-25.565208696707));
#29984=CARTESIAN_POINT('Ctrl Pts',(-26.1754950597027,25.4222050532839,-25.5590580598746));
#29985=CARTESIAN_POINT('Ctrl Pts',(-26.2322941484489,25.3398734371122,-25.5529074230421));
#29986=CARTESIAN_POINT('Ctrl Pts',(-26.2851230418963,25.2551281444375,-25.5467567862097));
#29987=CARTESIAN_POINT('Ctrl Pts',(-26.338008451162,25.1702921921019,-25.5405995694879));
#29988=CARTESIAN_POINT('Ctrl Pts',(-26.3869149534866,25.0830377763704,-25.5344423527661));
#29989=CARTESIAN_POINT('Ctrl Pts',(-26.4316321645472,24.9937791070921,-25.5282851360443));
#29990=CARTESIAN_POINT('Ctrl Pts',(-26.4763743231567,24.9044706407677,-25.5221244842365));
#29991=CARTESIAN_POINT('Ctrl Pts',(-26.5169223597245,24.8131560911232,-25.5159638324287));
#29992=CARTESIAN_POINT('Ctrl Pts',(-26.5531140382146,24.7202697688142,-25.5098031806209));
#29993=CARTESIAN_POINT('Ctrl Pts',(-26.5893662782528,24.6272280146571,-25.5036322198519));
#29994=CARTESIAN_POINT('Ctrl Pts',(-26.6212474603662,24.5326096460635,-25.4974612590828));
#29995=CARTESIAN_POINT('Ctrl Pts',(-26.6486451765087,24.4368643864872,-25.4912902983138));
#29996=CARTESIAN_POINT('Ctrl Pts',(-26.6695583676576,24.3637802321472,-25.4865798880933));
#29997=CARTESIAN_POINT('Ctrl Pts',(-26.6878602727366,24.2900398083783,-25.4818694778729));
#29998=CARTESIAN_POINT('Ctrl Pts',(-26.7035211438753,24.2158459676096,-25.4771590676524));
#29999=CARTESIAN_POINT('Ctrl Pts',(-26.7324039533253,24.0790128025634,-25.4684718190552));
#30000=CARTESIAN_POINT('Ctrl Pts',(-26.7523885214649,23.9402409635565,-25.4597845704581));
#30001=CARTESIAN_POINT('Ctrl Pts',(-26.7632725917776,23.8004917292665,-25.451097321861));
#30002=CARTESIAN_POINT('Ctrl Pts',(-26.7696722438977,23.7183215063795,-25.4459893643317));
#30003=CARTESIAN_POINT('Ctrl Pts',(-26.7729264349836,23.6358137368479,-25.4408814068025));
#30004=CARTESIAN_POINT('Ctrl Pts',(-26.7730012125181,23.5531684787983,-25.4357734492732));
#30005=CARTESIAN_POINT('Ctrl Pts',(-26.7730011889102,23.5531944548989,-25.4353089034207));
#30006=CARTESIAN_POINT('Ctrl Pts',(-26.7731884018712,23.3481108152563,-25.4238407640643));
#30007=CARTESIAN_POINT('Ctrl Pts',(-26.7538000984645,23.1434866085334,-25.4124470511572));
#30008=CARTESIAN_POINT('Ctrl Pts',(-26.7031666390037,22.8799922622032,-25.3967826797724));
#30009=CARTESIAN_POINT('Ctrl Pts',(-26.6894092282985,22.8182616518643,-25.3930429563939));
#30010=CARTESIAN_POINT('Ctrl Pts',(-26.668420407663,22.7356161449482,-25.3879222863631));
#30011=CARTESIAN_POINT('Ctrl Pts',(-26.6627762856602,22.7143104346675,-25.3865919026157));
#30012=CARTESIAN_POINT('Ctrl Pts',(-26.6542383834634,22.6833669565597,-25.3846440141879));
#30013=CARTESIAN_POINT('Ctrl Pts',(-26.651517222446,22.6736818941095,-25.3840320896982));
#30014=CARTESIAN_POINT('Ctrl Pts',(-26.6465449289241,22.6562976690975,-25.3829295945767));
#30015=CARTESIAN_POINT('Ctrl Pts',(-26.6443103054599,22.6485938400208,-25.3824395640204));
#30016=CARTESIAN_POINT('Ctrl Pts',(-26.6408780439607,22.6369241860975,-25.3816950300408));
#30017=CARTESIAN_POINT('Ctrl Pts',(-26.6397014703825,22.6329521561756,-25.3814412162738));
#30018=CARTESIAN_POINT('Ctrl Pts',(-26.6375688243138,22.6258031392673,-25.3809836765325));
#30019=CARTESIAN_POINT('Ctrl Pts',(-26.636615496696,22.6226253339657,-25.3807800407724));
#30020=CARTESIAN_POINT('Ctrl Pts',(-26.6346975093471,22.6162676363982,-25.3803721224825));
#30021=CARTESIAN_POINT('Ctrl Pts',(-26.6337328351289,22.6130877526885,-25.3801678396835));
#30022=CARTESIAN_POINT('Ctrl Pts',(-26.6310239654322,22.6042078881229,-25.3795966552453));
#30023=CARTESIAN_POINT('Ctrl Pts',(-26.629268877884,22.5985112676431,-25.3792293961564));
#30024=CARTESIAN_POINT('Ctrl Pts',(-26.622128657541,22.5755621820864,-25.3777464935016));
#30025=CARTESIAN_POINT('Ctrl Pts',(-26.6166143242975,22.5583505478229,-25.3766266048381));
#30026=CARTESIAN_POINT('Ctrl Pts',(-26.5236614073807,22.2764053979661,-25.3581519600213));
#30027=CARTESIAN_POINT('Ctrl Pts',(-26.4023970181992,22.024130081821,-25.339579901343));
#30028=CARTESIAN_POINT('Ctrl Pts',(-26.2280885577321,21.7566644747549,-25.3179710301184));
#30029=CARTESIAN_POINT('Ctrl Pts',(-26.2052948315316,21.7230923563477,-25.3152235755487));
#30030=CARTESIAN_POINT('Ctrl Pts',(-26.1601961409055,21.6592945322985,-25.3099429938384));
#30031=CARTESIAN_POINT('Ctrl Pts',(-26.1379844457675,21.6290103779702,-25.3074095324303));
#30032=CARTESIAN_POINT('Ctrl Pts',(-26.0569976219313,21.5225435138002,-25.2984211826418));
#30033=CARTESIAN_POINT('Ctrl Pts',(-25.9953419616863,21.4486066427533,-25.2920253528034));
#30034=CARTESIAN_POINT('Ctrl Pts',(-25.8994727031881,21.3435818525894,-25.2828292845965));
#30035=CARTESIAN_POINT('Ctrl Pts',(-25.8677548923741,21.3102939930612,-25.2798969970652));
#30036=CARTESIAN_POINT('Ctrl Pts',(-25.832586026379,21.2749313314308,-25.2767737138878));
#30037=CARTESIAN_POINT('Ctrl Pts',(-25.8298333296033,21.272173487519,-25.2765300816771));
#30038=CARTESIAN_POINT('Ctrl Pts',(-25.8253426346145,21.2676906854283,-25.2761339842759));
#30039=CARTESIAN_POINT('Ctrl Pts',(-25.8236076704964,21.2659627139585,-25.2759812825055));
#30040=CARTESIAN_POINT('Ctrl Pts',(-25.8202452034551,21.26262142416,-25.2756859765076));
#30041=CARTESIAN_POINT('Ctrl Pts',(-25.8186179465947,21.2610078618156,-25.275543352924));
#30042=CARTESIAN_POINT('Ctrl Pts',(-25.8156633477755,21.2580843715041,-25.2752849182419));
#30043=CARTESIAN_POINT('Ctrl Pts',(-25.8143365942525,21.25677386427,-25.2751690609383));
#30044=CARTESIAN_POINT('Ctrl Pts',(-25.811663806379,21.2541383845913,-25.2749360489257));
#30045=CARTESIAN_POINT('Ctrl Pts',(-25.8103177502107,21.2528134491734,-25.2748188970151));
#30046=CARTESIAN_POINT('Ctrl Pts',(-25.8064650454706,21.2490278592123,-25.2744841413567));
#30047=CARTESIAN_POINT('Ctrl Pts',(-25.8039555277778,21.2465701086411,-25.2742667680802));
#30048=CARTESIAN_POINT('Ctrl Pts',(-25.7931318544871,21.2360043231496,-25.2733321011948));
#30049=CARTESIAN_POINT('Ctrl Pts',(-25.7847777897391,21.22793702595,-25.2726179802339));
#30050=CARTESIAN_POINT('Ctrl Pts',(-25.6405526593777,21.090161476115,-25.2604099510848));
#30051=CARTESIAN_POINT('Ctrl Pts',(-25.49361760892,20.9725098359525,-25.2497899061814));
#30052=CARTESIAN_POINT('Ctrl Pts',(-25.2622466463587,20.8183454987195,-25.2342159687254));
#30053=CARTESIAN_POINT('Ctrl Pts',(-25.1851835457418,20.7715405176478,-25.2291984533894));
#30054=CARTESIAN_POINT('Ctrl Pts',(-25.0162539603779,20.678402767604,-25.2183763682211));
#30055=CARTESIAN_POINT('Ctrl Pts',(-24.9239294038489,20.6331150134832,-25.2125658290094));
#30056=CARTESIAN_POINT('Ctrl Pts',(-24.7538664296068,20.5595602659388,-25.2018725575941));
#30057=CARTESIAN_POINT('Ctrl Pts',(-24.6769047411481,20.5297261173178,-25.1970372714229));
#30058=CARTESIAN_POINT('Ctrl Pts',(-24.5587347299776,20.4890625084898,-25.1895663204952));
#30059=CARTESIAN_POINT('Ctrl Pts',(-24.5183145227767,20.4760410195271,-25.1870030473364));
#30060=CARTESIAN_POINT('Ctrl Pts',(-24.4703397101177,20.4616257468752,-25.1839476773876));
#30061=CARTESIAN_POINT('Ctrl Pts',(-24.4630214341635,20.4594551004631,-25.1834812468426));
#30062=CARTESIAN_POINT('Ctrl Pts',(-24.4517983873074,20.4561696106459,-25.182765383559));
#30063=CARTESIAN_POINT('Ctrl Pts',(-24.4478990713153,20.4550361027895,-25.1825165615587));
#30064=CARTESIAN_POINT('Ctrl Pts',(-24.4410963574338,20.4530725305681,-25.1820822842363));
#30065=CARTESIAN_POINT('Ctrl Pts',(-24.4381939095448,20.4522391697741,-25.1818969368485));
#30066=CARTESIAN_POINT('Ctrl Pts',(-24.432123918381,20.4505055640145,-25.1815091892792));
#30067=CARTESIAN_POINT('Ctrl Pts',(-24.4289561594791,20.4496060925323,-25.1813067640991));
#30068=CARTESIAN_POINT('Ctrl Pts',(-24.4201940160148,20.447132625693,-25.1807466502201));
#30069=CARTESIAN_POINT('Ctrl Pts',(-24.414596764343,20.4455689111071,-25.1803886268379));
#30070=CARTESIAN_POINT('Ctrl Pts',(-24.3926270071581,20.4394951954414,-25.1789824537228));
#30071=CARTESIAN_POINT('Ctrl Pts',(-24.3762234175929,20.4350995595521,-25.1779305905217));
#30072=CARTESIAN_POINT('Ctrl Pts',(-24.1014736756122,20.3637980891094,-25.1602778818559));
#30073=CARTESIAN_POINT('Ctrl Pts',(-23.8358927386007,20.3291214756929,-25.1425701657684));
#30074=CARTESIAN_POINT('Ctrl Pts',(-23.4267889288459,20.3267234742127,-25.1148939772119));
#30075=CARTESIAN_POINT('Ctrl Pts',(-23.2845310373082,20.3353220345913,-25.1052250138841));
#30076=CARTESIAN_POINT('Ctrl Pts',(-23.0537308282695,20.3647012457331,-25.0898361327789));
#30077=CARTESIAN_POINT('Ctrl Pts',(-22.9646668409626,20.3798639494307,-25.0839740286218));
#30078=CARTESIAN_POINT('Ctrl Pts',(-22.8703647349686,20.4000291128422,-25.0779301917035));
#30079=CARTESIAN_POINT('Ctrl Pts',(-22.8643845959251,20.4013257016508,-25.077547634101));
#30080=CARTESIAN_POINT('Ctrl Pts',(-22.8563549101249,20.4030906240935,-25.0770349530157));
#30081=CARTESIAN_POINT('Ctrl Pts',(-22.8543021274838,20.4035439311385,-25.0769039734312));
#30082=CARTESIAN_POINT('Ctrl Pts',(-22.8502524039958,20.4044423706066,-25.0766457508542));
#30083=CARTESIAN_POINT('Ctrl Pts',(-22.8482554408431,20.4048873966308,-25.0765185017903));
#30084=CARTESIAN_POINT('Ctrl Pts',(-22.8444162806151,20.4057467971586,-25.0762740276297));
#30085=CARTESIAN_POINT('Ctrl Pts',(-22.8425740291365,20.4061608878491,-25.076156786799));
#30086=CARTESIAN_POINT('Ctrl Pts',(-22.8383302133378,20.4071187072685,-25.0758868747397));
#30087=CARTESIAN_POINT('Ctrl Pts',(-22.8359289013411,20.4076635708469,-25.0757342694022));
#30088=CARTESIAN_POINT('Ctrl Pts',(-22.8295079310855,20.4091282446274,-25.075326529862));
#30089=CARTESIAN_POINT('Ctrl Pts',(-22.8254893928949,20.4100530222373,-25.0750716816159));
#30090=CARTESIAN_POINT('Ctrl Pts',(-22.7977834246291,20.4164849546489,-25.0733168548771));
#30091=CARTESIAN_POINT('Ctrl Pts',(-22.77415638964,20.422252556085,-25.071831649577));
#30092=CARTESIAN_POINT('Ctrl Pts',(-22.7484894056022,20.4288268668199,-25.0702282693014));
#30093=CARTESIAN_POINT('Ctrl Pts',(-22.746383285551,20.4293685981214,-25.070096776972));
#30094=CARTESIAN_POINT('Ctrl Pts',(-22.7382730603912,20.4314634458349,-25.0695907071709));
#30095=CARTESIAN_POINT('Ctrl Pts',(-22.7322728484797,20.4330317722651,-25.0692168903105));
#30096=CARTESIAN_POINT('Ctrl Pts',(-22.5844514960315,20.4721252959915,-25.0600212488412));
#30097=CARTESIAN_POINT('Ctrl Pts',(-22.4453345871329,20.5192781823821,-25.0516745944945));
#30098=CARTESIAN_POINT('Ctrl Pts',(-22.1582736097082,20.6389811651494,-25.0342009114188));
#30099=CARTESIAN_POINT('Ctrl Pts',(-22.0117053170849,20.7137091718695,-25.0251191020992));
#30100=CARTESIAN_POINT('Ctrl Pts',(-21.7695005183071,20.8615147519106,-25.0089992574562));
#30101=CARTESIAN_POINT('Ctrl Pts',(-21.6710754504718,20.9293599697798,-25.0020956390491));
#30102=CARTESIAN_POINT('Ctrl Pts',(-21.5497127840613,21.0233731794041,-24.992959904933));
#30103=CARTESIAN_POINT('Ctrl Pts',(-21.523109659365,21.0446647392237,-24.9909165609518));
#30104=CARTESIAN_POINT('Ctrl Pts',(-21.4806407506145,21.0797734422604,-24.9875848521638));
#30105=CARTESIAN_POINT('Ctrl Pts',(-21.464563511104,21.0933314640759,-24.9863069476716));
#30106=CARTESIAN_POINT('Ctrl Pts',(-21.445220533953,21.1099701785289,-24.9847486842183));
#30107=CARTESIAN_POINT('Ctrl Pts',(-21.441826778509,21.1129018146924,-24.9844744992205));
#30108=CARTESIAN_POINT('Ctrl Pts',(-21.4352760529614,21.1185844639965,-24.983943732195));
#30109=CARTESIAN_POINT('Ctrl Pts',(-21.4321183020021,21.1213345664682,-24.9836871882893));
#30110=CARTESIAN_POINT('Ctrl Pts',(-21.4266811764424,21.126088454664,-24.9832442661499));
#30111=CARTESIAN_POINT('Ctrl Pts',(-21.4243992504586,21.1280893250199,-24.9830580097833));
#30112=CARTESIAN_POINT('Ctrl Pts',(-21.4196911427847,21.1322293322858,-24.9826729660928));
#30113=CARTESIAN_POINT('Ctrl Pts',(-21.4172653490884,21.1343689038037,-24.9824741606752));
#30114=CARTESIAN_POINT('Ctrl Pts',(-21.4107097925491,21.140168532973,-24.9819357701278));
#30115=CARTESIAN_POINT('Ctrl Pts',(-21.4065862163756,21.1438355392585,-24.9815958932823));
#30116=CARTESIAN_POINT('Ctrl Pts',(-21.3913082819028,21.1574923046487,-24.9803320893177));
#30117=CARTESIAN_POINT('Ctrl Pts',(-21.3802143044725,21.1675490549554,-24.9794053356684));
#30118=CARTESIAN_POINT('Ctrl Pts',(-21.1902825530019,21.3421499556484,-24.9633806528413));
#30119=CARTESIAN_POINT('Ctrl Pts',(-21.0305897911249,21.5262891007911,-24.9473779817701));
#30120=CARTESIAN_POINT('Ctrl Pts',(-20.7889154821981,21.8784123272978,-24.9185566004384));
#30121=CARTESIAN_POINT('Ctrl Pts',(-20.6979079543708,22.0389063857813,-24.9059825873275));
#30122=CARTESIAN_POINT('Ctrl Pts',(-20.5993018170917,22.2538186249941,-24.8904472403405));
#30123=CARTESIAN_POINT('Ctrl Pts',(-20.5786572175354,22.3018643835983,-24.8870542862236));
#30124=CARTESIAN_POINT('Ctrl Pts',(-20.5496435745144,22.3741909401787,-24.88208666226));
#30125=CARTESIAN_POINT('Ctrl Pts',(-20.540381470176,22.3981018144832,-24.8804667693281));
#30126=CARTESIAN_POINT('Ctrl Pts',(-20.5298946739763,22.4261641905469,-24.8785937825932));
#30127=CARTESIAN_POINT('Ctrl Pts',(-20.5283920803275,22.4302098537728,-24.8783244397983));
#30128=CARTESIAN_POINT('Ctrl Pts',(-20.5261036578797,22.4364094510798,-24.8779127509367));
#30129=CARTESIAN_POINT('Ctrl Pts',(-20.5253120008632,22.4385612057224,-24.877770056116));
#30130=CARTESIAN_POINT('Ctrl Pts',(-20.5239424562059,22.4422959759785,-24.8775227215581));
#30131=CARTESIAN_POINT('Ctrl Pts',(-20.523363515203,22.4438785966043,-24.8774180183248));
#30132=CARTESIAN_POINT('Ctrl Pts',(-20.5221550884941,22.4471900574534,-24.8771991593359));
#30133=CARTESIAN_POINT('Ctrl Pts',(-20.5215258436894,22.4489189777687,-24.8770850183594));
#30134=CARTESIAN_POINT('Ctrl Pts',(-20.5199783451464,22.4531822591119,-24.8768038699544));
#30135=CARTESIAN_POINT('Ctrl Pts',(-20.5190617877949,22.4557172408671,-24.8766369646318));
#30136=CARTESIAN_POINT('Ctrl Pts',(-20.5154912957184,22.4656312629952,-24.8759852525025));
#30137=CARTESIAN_POINT('Ctrl Pts',(-20.5128610878374,22.4730189099971,-24.8755018556955));
#30138=CARTESIAN_POINT('Ctrl Pts',(-20.464922702181,22.609238283189,-24.8666285242348));
#30139=CARTESIAN_POINT('Ctrl Pts',(-20.4278152121157,22.7408307611289,-24.8587112864988));
#30140=CARTESIAN_POINT('Ctrl Pts',(-20.3608247917679,23.0531649242651,-24.8405838914187));
#30141=CARTESIAN_POINT('Ctrl Pts',(-20.3377637587829,23.2348726545533,-24.8305242899372));
#30142=CARTESIAN_POINT('Ctrl Pts',(-20.3246922209086,23.5520743529381,-24.8125820225287));
#30143=CARTESIAN_POINT('Ctrl Pts',(-20.3275837454163,23.6867915274818,-24.8048470393509));
#30144=CARTESIAN_POINT('Ctrl Pts',(-20.3435642375,23.8763907146123,-24.7935457820398));
#30145=CARTESIAN_POINT('Ctrl Pts',(-20.3496752336241,23.9317237731833,-24.7901982811708));
#30146=CARTESIAN_POINT('Ctrl Pts',(-20.3583145021751,23.9949040326001,-24.7863105455624));
#30147=CARTESIAN_POINT('Ctrl Pts',(-20.3594436192301,24.0029354491905,-24.7858151272651));
#30148=CARTESIAN_POINT('Ctrl Pts',(-20.3612030984382,24.0151169144062,-24.7850618431574));
#30149=CARTESIAN_POINT('Ctrl Pts',(-20.3618112775774,24.0192701761881,-24.7848046812701));
#30150=CARTESIAN_POINT('Ctrl Pts',(-20.3628733623185,24.0264256223609,-24.7843610565323));
#30151=CARTESIAN_POINT('Ctrl Pts',(-20.3633234007789,24.0294283825726,-24.7841747166687));
#30152=CARTESIAN_POINT('Ctrl Pts',(-20.3642610108956,24.0356245825048,-24.7837898427399));
#30153=CARTESIAN_POINT('Ctrl Pts',(-20.3647491418694,24.038817933248,-24.7835912910878));
#30154=CARTESIAN_POINT('Ctrl Pts',(-20.3659392769527,24.0465261813377,-24.7831115372972));
#30155=CARTESIAN_POINT('Ctrl Pts',(-20.3666460815882,24.0510403212438,-24.7828301828225));
#30156=CARTESIAN_POINT('Ctrl Pts',(-20.3692875461222,24.0676789213714,-24.7817916611449));
#30157=CARTESIAN_POINT('Ctrl Pts',(-20.3712818692017,24.0797936806887,-24.7810325986286));
#30158=CARTESIAN_POINT('Ctrl Pts',(-20.4046183674197,24.2753223754761,-24.7687338081732));
#30159=CARTESIAN_POINT('Ctrl Pts',(-20.4517119208864,24.4556611035921,-24.7566792777236));
#30160=CARTESIAN_POINT('Ctrl Pts',(-20.5759333105863,24.8046694572859,-24.7319714021758));
#30161=CARTESIAN_POINT('Ctrl Pts',(-20.6525832623123,24.972801138048,-24.7193716503923));
#30162=CARTESIAN_POINT('Ctrl Pts',(-20.7759911050168,25.1916088990411,-24.7025156064405));
#30163=CARTESIAN_POINT('Ctrl Pts',(-20.8105990912414,25.2487451401518,-24.6980709847025));
#30164=CARTESIAN_POINT('Ctrl Pts',(-20.8812051224731,25.3575323700152,-24.6895770141447));
#30165=CARTESIAN_POINT('Ctrl Pts',(-20.9169914727159,25.4092877555646,-24.6855214791563));
#30166=CARTESIAN_POINT('Ctrl Pts',(-20.9604302225336,25.468336456842,-24.6809074436844));
#30167=CARTESIAN_POINT('Ctrl Pts',(-20.9666282369265,25.4766769520849,-24.6802560372837));
#30168=CARTESIAN_POINT('Ctrl Pts',(-20.9748071527373,25.4875726165946,-24.6794056436001));
#30169=CARTESIAN_POINT('Ctrl Pts',(-20.9767516202334,25.4901548669365,-24.6792041446733));
#30170=CARTESIAN_POINT('Ctrl Pts',(-20.9799357772215,25.4943702102052,-24.6788752875817));
#30171=CARTESIAN_POINT('Ctrl Pts',(-20.9811731398142,25.4960050453752,-24.6787477657336));
#30172=CARTESIAN_POINT('Ctrl Pts',(-20.9835521528349,25.4991420327842,-24.6785031094168));
#30173=CARTESIAN_POINT('Ctrl Pts',(-20.9846935589217,25.5006443588757,-24.6783859586087));
#30174=CARTESIAN_POINT('Ctrl Pts',(-20.9873218890374,25.5040974845918,-24.6781167223467));
#30175=CARTESIAN_POINT('Ctrl Pts',(-20.9888097250308,25.5060475944042,-24.6779647017149));
#30176=CARTESIAN_POINT('Ctrl Pts',(-20.9935411057226,25.5122343655977,-24.6774824922253));
#30177=CARTESIAN_POINT('Ctrl Pts',(-20.9967929678628,25.5164646995712,-24.6771528902814));
#30178=CARTESIAN_POINT('Ctrl Pts',(-21.0246578149761,25.5525282463149,-24.6743438678715));
#30179=CARTESIAN_POINT('Ctrl Pts',(-21.0498558660914,25.5839077607909,-24.671905224204));
#30180=CARTESIAN_POINT('Ctrl Pts',(-21.0799522337295,25.6199818344024,-24.6690973586096));
#30181=CARTESIAN_POINT('Ctrl Pts',(-21.0842842821854,25.6251413341401,-24.6686956564226));
#30182=CARTESIAN_POINT('Ctrl Pts',(-21.0895053122892,25.6313201695628,-24.6682144109145));
#30183=CARTESIAN_POINT('Ctrl Pts',(-21.090378763121,25.6323525374314,-24.6681339976959));
#30184=CARTESIAN_POINT('Ctrl Pts',(-21.0950344255599,25.6378482397424,-24.6677058919929));
#30185=CARTESIAN_POINT('Ctrl Pts',(-21.098828159937,25.6423018474209,-24.6673588428888));
#30186=CARTESIAN_POINT('Ctrl Pts',(-21.1049678416876,25.6494698186711,-24.666800034592));
#30187=CARTESIAN_POINT('Ctrl Pts',(-21.1073062145871,25.6521906195225,-24.6665878671274));
#30188=CARTESIAN_POINT('Ctrl Pts',(-21.113142139006,25.6589580835634,-24.6660599847067));
#30189=CARTESIAN_POINT('Ctrl Pts',(-21.1166452415063,25.6629999677221,-24.6657445653324));
#30190=CARTESIAN_POINT('Ctrl Pts',(-21.1438216464234,25.6941988655711,-24.6633086188658));
#30191=CARTESIAN_POINT('Ctrl Pts',(-21.1679395541954,25.720966824405,-24.6612112363208));
#30192=CARTESIAN_POINT('Ctrl Pts',(-21.3509471070143,25.9173581750506,-24.6457183651113));
#30193=CARTESIAN_POINT('Ctrl Pts',(-21.5273273903961,26.0697606774814,-24.6330541793684));
#30194=CARTESIAN_POINT('Ctrl Pts',(-21.8239570215381,26.2746653433132,-24.6126352561625));
#30195=CARTESIAN_POINT('Ctrl Pts',(-21.9335721904794,26.3411056280582,-24.6052582349024));
#30196=CARTESIAN_POINT('Ctrl Pts',(-22.0562160936962,26.4057883835446,-24.5970160069381));
#30197=CARTESIAN_POINT('Ctrl Pts',(-22.0656142246213,26.410685883649,-24.5963845258621));
#30198=CARTESIAN_POINT('Ctrl Pts',(-22.0750360162151,26.4155367750037,-24.595751509546));
#30199=CARTESIAN_POINT('Origin',(-23.5502525316942,23.5502525316942,-77.3107734492734));
#30200=CARTESIAN_POINT('',(-22.0750360144199,26.4155367740794,-23.0992549867839));
#30201=CARTESIAN_POINT('',(-22.0750361484425,26.4155368430821,-23.3437344129902));
#30202=CARTESIAN_POINT('',(-22.0750360153461,26.4155367745563,-77.3107734492734));
#30203=CARTESIAN_POINT('',(-26.7730011959272,23.5473183053636,-23.9397396857875));
#30204=CARTESIAN_POINT('Ctrl Pts',(-22.0750360144199,26.4155367740794,-23.0992549867839));
#30205=CARTESIAN_POINT('Ctrl Pts',(-22.0526720052502,26.4040224694141,-23.1008603458253));
#30206=CARTESIAN_POINT('Ctrl Pts',(-22.0304419422344,26.3922458895206,-23.1024518991583));
#30207=CARTESIAN_POINT('Ctrl Pts',(-22.0032929933772,26.3774537839156,-23.1043883274086));
#30208=CARTESIAN_POINT('Ctrl Pts',(-21.9982428631065,26.3746846380804,-23.1047482203538));
#30209=CARTESIAN_POINT('Ctrl Pts',(-21.9911837266924,26.3707892408664,-23.1052508151255));
#30210=CARTESIAN_POINT('Ctrl Pts',(-21.9891685018808,26.3696743728632,-23.1053942410843));
#30211=CARTESIAN_POINT('Ctrl Pts',(-21.9854852714282,26.3676315667143,-23.1056562805497));
#30212=CARTESIAN_POINT('Ctrl Pts',(-21.9838168929055,26.3667043057108,-23.1057749377895));
#30213=CARTESIAN_POINT('Ctrl Pts',(-21.9804318188111,26.3648189915202,-23.1060156104344));
#30214=CARTESIAN_POINT('Ctrl Pts',(-21.9787151754853,26.3638608494001,-23.1061376198625));
#30215=CARTESIAN_POINT('Ctrl Pts',(-21.9745064460719,26.3615066993986,-23.1064366553964));
#30216=CARTESIAN_POINT('Ctrl Pts',(-21.9720153311895,26.3601089445529,-23.1066135683252));
#30217=CARTESIAN_POINT('Ctrl Pts',(-21.9629028630669,26.3549800328295,-23.1072604185072));
#30218=CARTESIAN_POINT('Ctrl Pts',(-21.9562927882141,26.3512287302806,-23.1077290646005));
#30219=CARTESIAN_POINT('Ctrl Pts',(-21.8041224907108,26.2641570021886,-23.1185060047682));
#30220=CARTESIAN_POINT('Ctrl Pts',(-21.6652493783781,26.1696090175664,-23.1280982957044));
#30221=CARTESIAN_POINT('Ctrl Pts',(-21.3790799817679,25.9401759256473,-23.1487362799999));
#30222=CARTESIAN_POINT('Ctrl Pts',(-21.235677483171,25.8015777694774,-23.1596934586764));
#30223=CARTESIAN_POINT('Ctrl Pts',(-21.0702570794957,25.6090734412315,-23.1742394009387));
#30224=CARTESIAN_POINT('Ctrl Pts',(-21.0356070445344,25.566605336247,-23.1774093606516));
#30225=CARTESIAN_POINT('Ctrl Pts',(-20.9891845055225,25.5066498009376,-23.1818481530357));
#30226=CARTESIAN_POINT('Ctrl Pts',(-20.9764744656409,25.4898984139694,-23.1830845046559));
#30227=CARTESIAN_POINT('Ctrl Pts',(-20.956437147721,25.4629461860943,-23.1850685601107));
#30228=CARTESIAN_POINT('Ctrl Pts',(-20.9490038800524,25.4528246611588,-23.1858124946643));
#30229=CARTESIAN_POINT('Ctrl Pts',(-20.9098721462823,25.398882832957,-23.1897717415704));
#30230=CARTESIAN_POINT('Ctrl Pts',(-20.8792228444592,25.3543152930603,-23.1930240305316));
#30231=CARTESIAN_POINT('Ctrl Pts',(-20.8449141634396,25.3016345935273,-23.1968550702407));
#30232=CARTESIAN_POINT('Ctrl Pts',(-20.840147809869,25.2942500109331,-23.1973917880099));
#30233=CARTESIAN_POINT('Ctrl Pts',(-20.8330949964117,25.2832242498736,-23.1981927353129));
#30234=CARTESIAN_POINT('Ctrl Pts',(-20.8307854908379,25.2795978011429,-23.1984561059475));
#30235=CARTESIAN_POINT('Ctrl Pts',(-20.8266819636738,25.273125782778,-23.1989260223214));
#30236=CARTESIAN_POINT('Ctrl Pts',(-20.8248851241249,25.2702820000202,-23.1991324630038));
#30237=CARTESIAN_POINT('Ctrl Pts',(-20.8211090458313,25.2642849865661,-23.199567728883));
#30238=CARTESIAN_POINT('Ctrl Pts',(-20.8191308132183,25.2611311309716,-23.1997965909635));
#30239=CARTESIAN_POINT('Ctrl Pts',(-20.8139263454462,25.2528017262641,-23.2004009035254));
#30240=CARTESIAN_POINT('Ctrl Pts',(-20.810709340469,25.2476204529389,-23.2007766944757));
#30241=CARTESIAN_POINT('Ctrl Pts',(-20.7965075665723,25.2246016803702,-23.2024457171014));
#30242=CARTESIAN_POINT('Ctrl Pts',(-20.7856823631863,25.206666777778,-23.2037448036639));
#30243=CARTESIAN_POINT('Ctrl Pts',(-20.7085360894879,25.0759898615199,-23.2132023369311));
#30244=CARTESIAN_POINT('Ctrl Pts',(-20.6489669286855,24.9594227849635,-23.2216043350849));
#30245=CARTESIAN_POINT('Ctrl Pts',(-20.5061810561957,24.6323255162996,-23.2450942772063));
#30246=CARTESIAN_POINT('Ctrl Pts',(-20.4377823232886,24.4161423954807,-23.2605675407608));
#30247=CARTESIAN_POINT('Ctrl Pts',(-20.3820984467936,24.1432649662729,-23.2792669845356));
#30248=CARTESIAN_POINT('Ctrl Pts',(-20.3728737988561,24.0916662810255,-23.2827643168317));
#30249=CARTESIAN_POINT('Ctrl Pts',(-20.3519589038958,23.955596953829,-23.291851815795));
#30250=CARTESIAN_POINT('Ctrl Pts',(-20.3423540112512,23.8708400634492,-23.2973770419077));
#30251=CARTESIAN_POINT('Ctrl Pts',(-20.3356585118087,23.7794751077061,-23.3031195551253));
#30252=CARTESIAN_POINT('Ctrl Pts',(-20.3352140922839,23.7731550592039,-23.3035156891557));
#30253=CARTESIAN_POINT('Ctrl Pts',(-20.3346226657071,23.7643744657246,-23.304064485965));
#30254=CARTESIAN_POINT('Ctrl Pts',(-20.3344598433802,23.7619150544676,-23.3042180317759));
#30255=CARTESIAN_POINT('Ctrl Pts',(-20.3341845214919,23.7576826939507,-23.3044819707126));
#30256=CARTESIAN_POINT('Ctrl Pts',(-20.3340706664254,23.7559098389113,-23.3045924404842));
#30257=CARTESIAN_POINT('Ctrl Pts',(-20.3338382123986,23.7522428554611,-23.3048207510061));
#30258=CARTESIAN_POINT('Ctrl Pts',(-20.3337198208707,23.7503487197704,-23.3049385793195));
#30259=CARTESIAN_POINT('Ctrl Pts',(-20.3334880305208,23.7465869590227,-23.3051723845295));
#30260=CARTESIAN_POINT('Ctrl Pts',(-20.3333745847555,23.7447193358178,-23.3052883642054));
#30261=CARTESIAN_POINT('Ctrl Pts',(-20.3329978407276,23.7384265658923,-23.3056788159374));
#30262=CARTESIAN_POINT('Ctrl Pts',(-20.3327420447994,23.7340009493014,-23.3059528650489));
#30263=CARTESIAN_POINT('Ctrl Pts',(-20.330912618885,23.701173745058,-23.3079816498569));
#30264=CARTESIAN_POINT('Ctrl Pts',(-20.3297058779552,23.6727518077291,-23.3097160531707));
#30265=CARTESIAN_POINT('Ctrl Pts',(-20.3269511859043,23.5784127480245,-23.3154105682177));
#30266=CARTESIAN_POINT('Ctrl Pts',(-20.327049529715,23.5124606501146,-23.3192907359446));
#30267=CARTESIAN_POINT('Ctrl Pts',(-20.3352371621147,23.2581378676011,-23.334021231277));
#30268=CARTESIAN_POINT('Ctrl Pts',(-20.3578234590084,23.0706055463776,-23.3444091301467));
#30269=CARTESIAN_POINT('Ctrl Pts',(-20.4279196131496,22.7377635052762,-23.3634774543496));
#30270=CARTESIAN_POINT('Ctrl Pts',(-20.4695876885442,22.5918167582764,-23.3720671587884));
#30271=CARTESIAN_POINT('Ctrl Pts',(-20.5241750661265,22.4416316695437,-23.3814550155393));
#30272=CARTESIAN_POINT('Ctrl Pts',(-20.5270107178045,22.433921945941,-23.3819384688577));
#30273=CARTESIAN_POINT('Ctrl Pts',(-20.5543047109259,22.3605803176069,-23.3865524052256));
#30274=CARTESIAN_POINT('Ctrl Pts',(-20.5808655039735,22.2957554736422,-23.3907450756816));
#30275=CARTESIAN_POINT('Ctrl Pts',(-20.613344061928,22.2233110149212,-23.3955805924083));
#30276=CARTESIAN_POINT('Ctrl Pts',(-20.6172098019913,22.2147880089344,-23.3961518718639));
#30277=CARTESIAN_POINT('Ctrl Pts',(-20.6229604040299,22.202254758996,-23.3969955157115));
#30278=CARTESIAN_POINT('Ctrl Pts',(-20.6248165247868,22.1982313169702,-23.3972668870566));
#30279=CARTESIAN_POINT('Ctrl Pts',(-20.6281087067295,22.1911334998293,-23.39774658335));
#30280=CARTESIAN_POINT('Ctrl Pts',(-20.6295413398934,22.188057534454,-23.3979547893603));
#30281=CARTESIAN_POINT('Ctrl Pts',(-20.6325149081688,22.1816993283513,-23.3983858310079));
#30282=CARTESIAN_POINT('Ctrl Pts',(-20.6340565293918,22.1784174154723,-23.3986086902226));
#30283=CARTESIAN_POINT('Ctrl Pts',(-20.6380205131122,22.1700154814129,-23.3991801748325));
#30284=CARTESIAN_POINT('Ctrl Pts',(-20.6404508334848,22.1648992477027,-23.3995290764575));
#30285=CARTESIAN_POINT('Ctrl Pts',(-20.6502732736223,22.144361234189,-23.4009333280311));
#30286=CARTESIAN_POINT('Ctrl Pts',(-20.6577745040162,22.1289922181322,-23.401992475539));
#30287=CARTESIAN_POINT('Ctrl Pts',(-20.7004942582236,22.0432042588119,-23.4079520153094));
#30288=CARTESIAN_POINT('Ctrl Pts',(-20.7381591809437,21.9740399989937,-23.4129381228677));
#30289=CARTESIAN_POINT('Ctrl Pts',(-20.8172861502717,21.8406184110363,-23.4229307101639));
#30290=CARTESIAN_POINT('Ctrl Pts',(-20.8585779155171,21.7763189272092,-23.4279289919953));
#30291=CARTESIAN_POINT('Ctrl Pts',(-21.0025744920654,21.5687059696429,-23.4446634374616));
#30292=CARTESIAN_POINT('Ctrl Pts',(-21.1147460351111,21.4323548253059,-23.4566555367521));
#30293=CARTESIAN_POINT('Ctrl Pts',(-21.3513725353846,21.188519213391,-23.4795925760803));
#30294=CARTESIAN_POINT('Ctrl Pts',(-21.4740362523306,21.0799898051002,-23.4905119516601));
#30295=CARTESIAN_POINT('Ctrl Pts',(-21.6120169235371,20.9754805025922,-23.5013991362776));
#30296=CARTESIAN_POINT('Ctrl Pts',(-21.619634798213,20.9697635378817,-23.5019959719635));
#30297=CARTESIAN_POINT('Ctrl Pts',(-21.6298830023823,20.962143381919,-23.502793088914));
#30298=CARTESIAN_POINT('Ctrl Pts',(-21.6324909246131,20.9602103469244,-23.502995435553));
#30299=CARTESIAN_POINT('Ctrl Pts',(-21.636577585143,20.9571908030581,-23.503311727895));
#30300=CARTESIAN_POINT('Ctrl Pts',(-21.6380543290206,20.9561016179446,-23.5034258616197));
#30301=CARTESIAN_POINT('Ctrl Pts',(-21.6408898541461,20.9540139888709,-23.5036447024369));
#30302=CARTESIAN_POINT('Ctrl Pts',(-21.6422484799371,20.9530153565119,-23.5037494224437));
#30303=CARTESIAN_POINT('Ctrl Pts',(-21.6454640087084,20.9506557272755,-23.5039969471388));
#30304=CARTESIAN_POINT('Ctrl Pts',(-21.647321584708,20.9492956550959,-23.5041396864265));
#30305=CARTESIAN_POINT('Ctrl Pts',(-21.6527015468777,20.9453654256284,-23.50455236521));
#30306=CARTESIAN_POINT('Ctrl Pts',(-21.6562277113733,20.9428004121212,-23.5048219454728));
#30307=CARTESIAN_POINT('Ctrl Pts',(-21.6813580722248,20.9245978832095,-23.5067368871061));
#30308=CARTESIAN_POINT('Ctrl Pts',(-21.7031512656833,20.909221320502,-23.5083644142925));
#30309=CARTESIAN_POINT('Ctrl Pts',(-21.7406046323372,20.8834858746942,-23.5111101663504));
#30310=CARTESIAN_POINT('Ctrl Pts',(-21.7561685422695,20.8729903862415,-23.5122363947064));
#30311=CARTESIAN_POINT('Ctrl Pts',(-21.8399782720328,20.8175325562861,-23.5182274075555));
#30312=CARTESIAN_POINT('Ctrl Pts',(-21.9098290128302,20.7750391717824,-23.5229619072411));
#30313=CARTESIAN_POINT('Ctrl Pts',(-22.0940734020842,20.6723451183414,-23.5349951245099));
#30314=CARTESIAN_POINT('Ctrl Pts',(-22.2106064329151,20.6162860039805,-23.5421785095639));
#30315=CARTESIAN_POINT('Ctrl Pts',(-22.5588791986188,20.4738353558232,-23.5632159096264));
#30316=CARTESIAN_POINT('Ctrl Pts',(-22.7975225493418,20.4069205050357,-23.5771737610186));
#30317=CARTESIAN_POINT('Ctrl Pts',(-23.0432947225784,20.3676254979143,-23.5922640621125));
#30318=CARTESIAN_POINT('Ctrl Pts',(-23.0451407231895,20.3673319990299,-23.5923774403421));
#30319=CARTESIAN_POINT('Ctrl Pts',(-23.0615135198418,20.364743461565,-23.5933833390404));
#30320=CARTESIAN_POINT('Ctrl Pts',(-23.076055423014,20.3625463111515,-23.59427891268));
#30321=CARTESIAN_POINT('Ctrl Pts',(-23.0960326882598,20.3596676489539,-23.595512349508));
#30322=CARTESIAN_POINT('Ctrl Pts',(-23.101455662634,20.3589003214428,-23.59584749003));
#30323=CARTESIAN_POINT('Ctrl Pts',(-23.110076159562,20.3577029654525,-23.5963807472094));
#30324=CARTESIAN_POINT('Ctrl Pts',(-23.1132724342129,20.3572639056925,-23.5965785774332));
#30325=CARTESIAN_POINT('Ctrl Pts',(-23.1194792363821,20.3564207958164,-23.5969629591715));
#30326=CARTESIAN_POINT('Ctrl Pts',(-23.122489687642,20.356016200706,-23.5971494932159));
#30327=CARTESIAN_POINT('Ctrl Pts',(-23.1296713298563,20.3550613454243,-23.5975947225523));
#30328=CARTESIAN_POINT('Ctrl Pts',(-23.1338430272395,20.3545149973389,-23.5978535413942));
#30329=CARTESIAN_POINT('Ctrl Pts',(-23.1424909710813,20.3533996366139,-23.5983904772561));
#30330=CARTESIAN_POINT('Ctrl Pts',(-23.146967364325,20.3528318529995,-23.5986686326294));
#30331=CARTESIAN_POINT('Ctrl Pts',(-23.1727640578846,20.3496148469964,-23.6002728994812));
#30332=CARTESIAN_POINT('Ctrl Pts',(-23.1941088221092,20.3471695232961,-23.6016054439138));
#30333=CARTESIAN_POINT('Ctrl Pts',(-23.331948350839,20.3327729852343,-23.6102453931805));
#30334=CARTESIAN_POINT('Ctrl Pts',(-23.4489834350858,20.3269668961474,-23.6177457480732));
#30335=CARTESIAN_POINT('Ctrl Pts',(-23.5918469541447,20.3276678158969,-23.6271060223113));
#30336=CARTESIAN_POINT('Ctrl Pts',(-23.6176271013464,20.3281037201314,-23.6288030111484));
#30337=CARTESIAN_POINT('Ctrl Pts',(-23.7992293307109,20.3333547118536,-23.6408102743609));
#30338=CARTESIAN_POINT('Ctrl Pts',(-23.9545180558525,20.349161448779,-23.6513683593087));
#30339=CARTESIAN_POINT('Ctrl Pts',(-24.2933576937108,20.408705929475,-23.6746481218824));
#30340=CARTESIAN_POINT('Ctrl Pts',(-24.4754912276071,20.4574428319542,-23.6873247070297));
#30341=CARTESIAN_POINT('Ctrl Pts',(-24.6632907085622,20.5257857751049,-23.6999206682697));
#30342=CARTESIAN_POINT('Ctrl Pts',(-24.6742112107683,20.5298270579421,-23.700651282035));
#30343=CARTESIAN_POINT('Ctrl Pts',(-24.6884006392453,20.5351656655093,-23.701597973782));
#30344=CARTESIAN_POINT('Ctrl Pts',(-24.6916895019339,20.5364092098517,-23.7018172164006));
#30345=CARTESIAN_POINT('Ctrl Pts',(-24.6967425088693,20.5383292483968,-23.7021537701781));
#30346=CARTESIAN_POINT('Ctrl Pts',(-24.6985080910102,20.5390019106441,-23.7022713115765));
#30347=CARTESIAN_POINT('Ctrl Pts',(-24.7020150150549,20.5403415327603,-23.7025046706367));
#30348=CARTESIAN_POINT('Ctrl Pts',(-24.7037563597892,20.5410084475123,-23.7026204896939));
#30349=CARTESIAN_POINT('Ctrl Pts',(-24.7076351717219,20.5424978488391,-23.7028783543432));
#30350=CARTESIAN_POINT('Ctrl Pts',(-24.7097723364268,20.5433211007856,-23.7030203526736));
#30351=CARTESIAN_POINT('Ctrl Pts',(-24.7141909275168,20.5450285866354,-23.7033137702766));
#30352=CARTESIAN_POINT('Ctrl Pts',(-24.7164722291671,20.54591314232,-23.7034651700428));
#30353=CARTESIAN_POINT('Ctrl Pts',(-24.7288682872509,20.5507358572257,-23.7042873594953));
#30354=CARTESIAN_POINT('Ctrl Pts',(-24.7389642676682,20.5547225624952,-23.7049552490516));
#30355=CARTESIAN_POINT('Ctrl Pts',(-24.7652369262736,20.5652508651911,-23.7066892161213));
#30356=CARTESIAN_POINT('Ctrl Pts',(-24.7813811958475,20.5718730610906,-23.7077506745688));
#30357=CARTESIAN_POINT('Ctrl Pts',(-24.8338768826158,20.593905981155,-23.7111914285813));
#30358=CARTESIAN_POINT('Ctrl Pts',(-24.8700003717419,20.6098542019597,-23.7135421767373));
#30359=CARTESIAN_POINT('Ctrl Pts',(-24.9867121830484,20.6639658680672,-23.7211103545583));
#30360=CARTESIAN_POINT('Ctrl Pts',(-25.066015557521,20.7048120328583,-23.7262109146711));
#30361=CARTESIAN_POINT('Ctrl Pts',(-25.2100786963827,20.7867481608396,-23.7355775440997));
#30362=CARTESIAN_POINT('Ctrl Pts',(-25.2752610823137,20.8269594419621,-23.7398565314771));
#30363=CARTESIAN_POINT('Ctrl Pts',(-25.5637921702891,21.0194748815147,-23.7592381835299));
#30364=CARTESIAN_POINT('Ctrl Pts',(-25.7688317937022,21.1971572815913,-23.7743667659568));
#30365=CARTESIAN_POINT('Ctrl Pts',(-25.9609057437737,21.4112874541552,-23.7917933946624));
#30366=CARTESIAN_POINT('Ctrl Pts',(-25.9724225127965,21.4243378871351,-23.7928521842482));
#30367=CARTESIAN_POINT('Ctrl Pts',(-25.9876814368424,21.4419137643161,-23.7942740129781));
#30368=CARTESIAN_POINT('Ctrl Pts',(-25.991517904435,21.4463572384781,-23.7946331272622));
#30369=CARTESIAN_POINT('Ctrl Pts',(-25.9974950197168,21.4533184153263,-23.7951951868065));
#30370=CARTESIAN_POINT('Ctrl Pts',(-25.9996439855587,21.4558289859004,-23.7953977878822));
#30371=CARTESIAN_POINT('Ctrl Pts',(-26.0037476673929,21.4606381447685,-23.7957856801245));
#30372=CARTESIAN_POINT('Ctrl Pts',(-26.0057030253743,21.4629361829029,-23.7959709445524));
#30373=CARTESIAN_POINT('Ctrl Pts',(-26.0102677180874,21.4683161368726,-23.7964044640518));
#30374=CARTESIAN_POINT('Ctrl Pts',(-26.0128744890458,21.4714002126723,-23.7966528241015));
#30375=CARTESIAN_POINT('Ctrl Pts',(-26.0203245733942,21.4802480991828,-23.7973649012666));
#30376=CARTESIAN_POINT('Ctrl Pts',(-26.0251534714505,21.4860239642489,-23.797829207574));
#30377=CARTESIAN_POINT('Ctrl Pts',(-26.0557543723189,21.5228875587062,-23.8007892573681));
#30378=CARTESIAN_POINT('Ctrl Pts',(-26.0809594311276,21.5544392746789,-23.8033078989538));
#30379=CARTESIAN_POINT('Ctrl Pts',(-26.244414824835,21.7671289644243,-23.8201978888315));
#30380=CARTESIAN_POINT('Ctrl Pts',(-26.3636864802293,21.9619851869276,-23.8353240067263));
#30381=CARTESIAN_POINT('Ctrl Pts',(-26.4777808904536,22.2022343826553,-23.853299922116));
#30382=CARTESIAN_POINT('Ctrl Pts',(-26.493544964916,22.2370104166826,-23.8558846631623));
#30383=CARTESIAN_POINT('Ctrl Pts',(-26.5757446364894,22.427265028808,-23.8699136662745));
#30384=CARTESIAN_POINT('Ctrl Pts',(-26.6304903866062,22.587522776766,-23.8813450294571));
#30385=CARTESIAN_POINT('Ctrl Pts',(-26.6821308760925,22.7893365361344,-23.894757065339));
#30386=CARTESIAN_POINT('Ctrl Pts',(-26.6911576956937,22.8275006976044,-23.8972506216658));
#30387=CARTESIAN_POINT('Ctrl Pts',(-26.7004989772834,22.8704822495638,-23.900003971944));
#30388=CARTESIAN_POINT('Ctrl Pts',(-26.7015014226486,22.8751445904222,-23.9003019142834));
#30389=CARTESIAN_POINT('Ctrl Pts',(-26.7029947639759,22.8821658722308,-23.9007494982689));
#30390=CARTESIAN_POINT('Ctrl Pts',(-26.7034933638686,22.8845231405997,-23.9008995793385));
#30391=CARTESIAN_POINT('Ctrl Pts',(-26.7043520109571,22.8886052374062,-23.9011591490832));
#30392=CARTESIAN_POINT('Ctrl Pts',(-26.7047132871157,22.8903298016229,-23.9012687086991));
#30393=CARTESIAN_POINT('Ctrl Pts',(-26.7054627769787,22.8939221956383,-23.9014967181431));
#30394=CARTESIAN_POINT('Ctrl Pts',(-26.7058507460793,22.8957900718362,-23.9016151532709));
#30395=CARTESIAN_POINT('Ctrl Pts',(-26.7066195734819,22.8995081668616,-23.9018506688271));
#30396=CARTESIAN_POINT('Ctrl Pts',(-26.7070004645134,22.9013583804411,-23.901967751257));
#30397=CARTESIAN_POINT('Ctrl Pts',(-26.7078884691636,22.9056912316447,-23.9022416674573));
#30398=CARTESIAN_POINT('Ctrl Pts',(-26.7083942829245,22.9081741390036,-23.902398426545));
#30399=CARTESIAN_POINT('Ctrl Pts',(-26.7097109438724,22.9146764800406,-23.9028084193512));
#30400=CARTESIAN_POINT('Ctrl Pts',(-26.7105170524914,22.9186968850994,-23.9030613840234));
#30401=CARTESIAN_POINT('Ctrl Pts',(-26.7521445500613,23.1283862502783,-23.9162277483037));
#30402=CARTESIAN_POINT('Ctrl Pts',(-26.7728102336783,23.3375787477034,-23.9280086774442));
#30403=CARTESIAN_POINT('Ctrl Pts',(-26.7730011959272,23.5473183053636,-23.9397396857875));
#30404=CARTESIAN_POINT('Ctrl Pts',(-26.7730011946114,23.5473168605001,-23.9397396049744));
#30405=CARTESIAN_POINT('Ctrl Pts',(-26.7731913401487,23.7560566122004,-23.9514146933273));
#30406=CARTESIAN_POINT('Ctrl Pts',(-26.7531018191501,23.9643123818198,-23.9630020629255));
#30407=CARTESIAN_POINT('Ctrl Pts',(-26.7009884365783,24.2306218430946,-23.9788500787034));
#30408=CARTESIAN_POINT('Ctrl Pts',(-26.6871740276188,24.2917118419737,-23.9825546230068));
#30409=CARTESIAN_POINT('Ctrl Pts',(-26.6661438042863,24.3735494892528,-23.9876295540581));
#30410=CARTESIAN_POINT('Ctrl Pts',(-26.6604825235153,24.3946846870221,-23.9889503815506));
#30411=CARTESIAN_POINT('Ctrl Pts',(-26.6519194653666,24.4253981801862,-23.9908853337584));
#30412=CARTESIAN_POINT('Ctrl Pts',(-26.6491875112965,24.4350234976433,-23.9914939643327));
#30413=CARTESIAN_POINT('Ctrl Pts',(-26.6441945082637,24.4523081755506,-23.9925910053368));
#30414=CARTESIAN_POINT('Ctrl Pts',(-26.6419497195621,24.4599721784601,-23.9930788834171));
#30415=CARTESIAN_POINT('Ctrl Pts',(-26.6384994033316,24.4715917316363,-23.9938207979259));
#30416=CARTESIAN_POINT('Ctrl Pts',(-26.6373146991872,24.475553474798,-23.9940741520627));
#30417=CARTESIAN_POINT('Ctrl Pts',(-26.6351659572365,24.4826889753866,-23.9945311845607));
#30418=CARTESIAN_POINT('Ctrl Pts',(-26.6342046366951,24.4858635505183,-23.9947347735429));
#30419=CARTESIAN_POINT('Ctrl Pts',(-26.6322693770049,24.4922189823462,-23.9951428692646));
#30420=CARTESIAN_POINT('Ctrl Pts',(-26.6312954103363,24.495399826443,-23.9953473767017));
#30421=CARTESIAN_POINT('Ctrl Pts',(-26.6285569963222,24.5042939039249,-23.9959199348474));
#30422=CARTESIAN_POINT('Ctrl Pts',(-26.6267815775774,24.5100037212961,-23.9962883458997));
#30423=CARTESIAN_POINT('Ctrl Pts',(-26.6195334212119,24.5330873004436,-23.9977811819743));
#30424=CARTESIAN_POINT('Ctrl Pts',(-26.6139294050163,24.550419195487,-23.9989099238953));
#30425=CARTESIAN_POINT('Ctrl Pts',(-26.519397830105,24.8345320628341,-24.017545087222));
#30426=CARTESIAN_POINT('Ctrl Pts',(-26.3960942803446,25.0885346291411,-24.0362920090593));
#30427=CARTESIAN_POINT('Ctrl Pts',(-26.2192915525039,25.3568988811205,-24.0580453556523));
#30428=CARTESIAN_POINT('Ctrl Pts',(-26.1965005650715,25.3901198356431,-24.0607728054594));
#30429=CARTESIAN_POINT('Ctrl Pts',(-26.151527219039,25.4531095828278,-24.0660027638298));
#30430=CARTESIAN_POINT('Ctrl Pts',(-26.1294412712494,25.4829399032005,-24.0685057064869));
#30431=CARTESIAN_POINT('Ctrl Pts',(-26.048824160954,25.5879814055165,-24.0773992275354));
#30432=CARTESIAN_POINT('Ctrl Pts',(-25.9874740112576,25.6609759905915,-24.0837302108687));
#30433=CARTESIAN_POINT('Ctrl Pts',(-25.892135588897,25.7647000913621,-24.0928360104573));
#30434=CARTESIAN_POINT('Ctrl Pts',(-25.8605868521906,25.7975954316597,-24.0957412233313));
#30435=CARTESIAN_POINT('Ctrl Pts',(-25.825749706611,25.8324102111203,-24.098824215181));
#30436=CARTESIAN_POINT('Ctrl Pts',(-25.8231459242318,25.8350034356866,-24.0990539063354));
#30437=CARTESIAN_POINT('Ctrl Pts',(-25.8188658191795,25.8392516280609,-24.0994302579395));
#30438=CARTESIAN_POINT('Ctrl Pts',(-25.8171921163905,25.8409092128108,-24.0995771235987));
#30439=CARTESIAN_POINT('Ctrl Pts',(-25.813934097109,25.8441287887592,-24.099862418485));
#30440=CARTESIAN_POINT('Ctrl Pts',(-25.8123499781645,25.8456909767565,-24.1000008632961));
#30441=CARTESIAN_POINT('Ctrl Pts',(-25.8095674495811,25.8484293055243,-24.100243565293));
#30442=CARTESIAN_POINT('Ctrl Pts',(-25.8083697432332,25.8496061454182,-24.10034787822));
#30443=CARTESIAN_POINT('Ctrl Pts',(-25.8058301439159,25.85209760176,-24.1005687331212));
#30444=CARTESIAN_POINT('Ctrl Pts',(-25.8044880251404,25.8534119772111,-24.1006852559316));
#30445=CARTESIAN_POINT('Ctrl Pts',(-25.8006689998049,25.8571455222679,-24.1010162759714));
#30446=CARTESIAN_POINT('Ctrl Pts',(-25.7981893333185,25.8595618843087,-24.1012305508906));
#30447=CARTESIAN_POINT('Ctrl Pts',(-25.7876748376399,25.8697749683601,-24.1021363983417));
#30448=CARTESIAN_POINT('Ctrl Pts',(-25.779603177107,25.8775339108661,-24.1028250344881));
#30449=CARTESIAN_POINT('Ctrl Pts',(-25.6369681623953,26.0132198365096,-24.1148793439844));
#30450=CARTESIAN_POINT('Ctrl Pts',(-25.4916150674948,26.1293460963654,-24.1253889290192));
#30451=CARTESIAN_POINT('Ctrl Pts',(-25.2605723914126,26.2832669251856,-24.1409456774259));
#30452=CARTESIAN_POINT('Ctrl Pts',(-25.1819532705439,26.3309205124581,-24.1460606515053));
#30453=CARTESIAN_POINT('Ctrl Pts',(-25.0090674825753,26.4258522193989,-24.1571241608869));
#30454=CARTESIAN_POINT('Ctrl Pts',(-24.9143034855469,26.4719947646665,-24.1630791476204));
#30455=CARTESIAN_POINT('Ctrl Pts',(-24.742166867768,26.5456093841202,-24.1738904336621));
#30456=CARTESIAN_POINT('Ctrl Pts',(-24.6656844564941,26.5749231725428,-24.1786914958999));
#30457=CARTESIAN_POINT('Ctrl Pts',(-24.5488533596312,26.6146674686757,-24.1860723820432));
#30458=CARTESIAN_POINT('Ctrl Pts',(-24.5092802455146,26.6272816375021,-24.1885801440985));
#30459=CARTESIAN_POINT('Ctrl Pts',(-24.462204149314,26.6412910899979,-24.1915760180743));
#30460=CARTESIAN_POINT('Ctrl Pts',(-24.4549249562355,26.6434293653915,-24.1920396106293));
#30461=CARTESIAN_POINT('Ctrl Pts',(-24.4437478933156,26.6466698176789,-24.1927520112161));
#30462=CARTESIAN_POINT('Ctrl Pts',(-24.4398553484388,26.6477903923804,-24.1930002176856));
#30463=CARTESIAN_POINT('Ctrl Pts',(-24.4330583895921,26.6497332126272,-24.1934338089761));
#30464=CARTESIAN_POINT('Ctrl Pts',(-24.4301549075182,26.6505587235302,-24.1936190869576));
#30465=CARTESIAN_POINT('Ctrl Pts',(-24.4240767438306,26.6522776259771,-24.194007074424));
#30466=CARTESIAN_POINT('Ctrl Pts',(-24.4209018435775,26.6531702255538,-24.1942098094914));
#30467=CARTESIAN_POINT('Ctrl Pts',(-24.4121038877988,26.6556291392311,-24.194771809376));
#30468=CARTESIAN_POINT('Ctrl Pts',(-24.4064779591219,26.6571850464691,-24.1951314127393));
#30469=CARTESIAN_POINT('Ctrl Pts',(-24.3842907345081,26.6632563068459,-24.1965505160643));
#30470=CARTESIAN_POINT('Ctrl Pts',(-24.3676979352611,26.6676545304265,-24.1976138164549));
#30471=CARTESIAN_POINT('Ctrl Pts',(-24.091284638085,26.7385643546634,-24.215362586379));
#30472=CARTESIAN_POINT('Ctrl Pts',(-23.8242531776045,26.772504814028,-24.2331668575916));
#30473=CARTESIAN_POINT('Ctrl Pts',(-23.4214272906506,26.7732445289567,-24.2604203146326));
#30474=CARTESIAN_POINT('Ctrl Pts',(-23.2867965958626,26.7650413154186,-24.2695682297704));
#30475=CARTESIAN_POINT('Ctrl Pts',(-23.0924240080346,26.7409022095162,-24.2825541124644));
#30476=CARTESIAN_POINT('Ctrl Pts',(-23.0319996262432,26.7316464430765,-24.2865583138494));
#30477=CARTESIAN_POINT('Ctrl Pts',(-22.9349367916642,26.713939252274,-24.292900675658));
#30478=CARTESIAN_POINT('Ctrl Pts',(-22.8981207296166,26.7065559938886,-24.2952851960947));
#30479=CARTESIAN_POINT('Ctrl Pts',(-22.8568181674232,26.6975193984223,-24.2979300194087));
#30480=CARTESIAN_POINT('Ctrl Pts',(-22.8521983699295,26.6964979664753,-24.2982254208128));
#30481=CARTESIAN_POINT('Ctrl Pts',(-22.8457234806042,26.6950514124651,-24.2986388234941));
#30482=CARTESIAN_POINT('Ctrl Pts',(-22.8438665197796,26.6946348218338,-24.2987573136612));
#30483=CARTESIAN_POINT('Ctrl Pts',(-22.8401408995587,26.6937955492028,-24.2989948957758));
#30484=CARTESIAN_POINT('Ctrl Pts',(-22.838272243399,26.6933728447224,-24.2991139865327));
#30485=CARTESIAN_POINT('Ctrl Pts',(-22.8346953969855,26.6925603809119,-24.2993418000708));
#30486=CARTESIAN_POINT('Ctrl Pts',(-22.8329871501063,26.6921708954809,-24.2994505386666));
#30487=CARTESIAN_POINT('Ctrl Pts',(-22.8289682914225,26.6912511352162,-24.2997062161781));
#30488=CARTESIAN_POINT('Ctrl Pts',(-22.826657941614,26.690719702655,-24.2998530878346));
#30489=CARTESIAN_POINT('Ctrl Pts',(-22.8198492723732,26.6891456428286,-24.300285599877));
#30490=CARTESIAN_POINT('Ctrl Pts',(-22.8153525805544,26.6880958908815,-24.3005708305936));
#30491=CARTESIAN_POINT('Ctrl Pts',(-22.7767206179296,26.6789896669431,-24.3030178488451));
#30492=CARTESIAN_POINT('Ctrl Pts',(-22.7427150276733,26.6703857193908,-24.3051486259031));
#30493=CARTESIAN_POINT('Ctrl Pts',(-22.5714913024336,26.6240763784092,-24.3157910506227));
#30494=CARTESIAN_POINT('Ctrl Pts',(-22.4367224791473,26.5778632490605,-24.3238888879124));
#30495=CARTESIAN_POINT('Ctrl Pts',(-22.2272216684074,26.4901330316552,-24.336652316664));
#30496=CARTESIAN_POINT('Ctrl Pts',(-22.1503628003474,26.4543194309421,-24.3413741372416));
#30497=CARTESIAN_POINT('Ctrl Pts',(-22.0750358381979,26.41553668335,-24.3461133775544));
#30498=CARTESIAN_POINT('Ctrl Pts',(-22.0750360162151,26.4155367750037,-24.595751509546));
#30499=CARTESIAN_POINT('Ctrl Pts',(-22.1135901637226,26.4353867131996,-24.5931611949348));
#30500=CARTESIAN_POINT('Ctrl Pts',(-22.1525404942053,26.4544562058755,-24.5905450872213));
#30501=CARTESIAN_POINT('Ctrl Pts',(-22.1992285932744,26.4761571518567,-24.5874060765246));
#30502=CARTESIAN_POINT('Ctrl Pts',(-22.2066066639115,26.4795526714133,-24.5869099316408));
#30503=CARTESIAN_POINT('Ctrl Pts',(-22.2177862503386,26.4846465929852,-24.5861579857106));
#30504=CARTESIAN_POINT('Ctrl Pts',(-22.2215783899634,26.4863655953767,-24.5859028954903));
#30505=CARTESIAN_POINT('Ctrl Pts',(-22.2281375372298,26.4893235916303,-24.5854616203673));
#30506=CARTESIAN_POINT('Ctrl Pts',(-22.2309029882116,26.490566041501,-24.5852755547004));
#30507=CARTESIAN_POINT('Ctrl Pts',(-22.2366315793422,26.4931300491559,-24.5848900866926));
#30508=CARTESIAN_POINT('Ctrl Pts',(-22.2395949693015,26.4944510377824,-24.584690665037));
#30509=CARTESIAN_POINT('Ctrl Pts',(-22.246783399311,26.4976424164554,-24.5842068684607));
#30510=CARTESIAN_POINT('Ctrl Pts',(-22.2510104682009,26.4995081957512,-24.5839223356345));
#30511=CARTESIAN_POINT('Ctrl Pts',(-22.2667842902624,26.5064300851794,-24.5828603989528));
#30512=CARTESIAN_POINT('Ctrl Pts',(-22.2783565466571,26.5114274759495,-24.5820809878546));
#30513=CARTESIAN_POINT('Ctrl Pts',(-22.4759157260681,26.5953701807305,-24.5687684308176));
#30514=CARTESIAN_POINT('Ctrl Pts',(-22.6688550547314,26.6567057686386,-24.5556235351217));
#30515=CARTESIAN_POINT('Ctrl Pts',(-23.1550784418745,26.7623114966141,-24.5223063464347));
#30516=CARTESIAN_POINT('Ctrl Pts',(-23.4511820654088,26.7850140077257,-24.5017867825422));
#30517=CARTESIAN_POINT('Ctrl Pts',(-23.7544767040227,26.7665358265135,-24.4826244287114));
#30518=CARTESIAN_POINT('Ctrl Pts',(-23.762716842461,26.7660020034705,-24.4821053352034));
#30519=CARTESIAN_POINT('Ctrl Pts',(-23.7769695461287,26.7650236438852,-24.4812102187402));
#30520=CARTESIAN_POINT('Ctrl Pts',(-23.7829830373137,26.7645938983768,-24.4808333971234));
#30521=CARTESIAN_POINT('Ctrl Pts',(-23.7915880354677,26.7639546797248,-24.4802954290968));
#30522=CARTESIAN_POINT('Ctrl Pts',(-23.7941805030643,26.7637589447166,-24.4801335147024));
#30523=CARTESIAN_POINT('Ctrl Pts',(-23.7986804902654,26.7634137123425,-24.4798527489413));
#30524=CARTESIAN_POINT('Ctrl Pts',(-23.8005881163156,26.7632656531378,-24.4797338159228));
#30525=CARTESIAN_POINT('Ctrl Pts',(-23.8042454445681,26.7629785149475,-24.4795059672133));
#30526=CARTESIAN_POINT('Ctrl Pts',(-23.805995162196,26.7628397056464,-24.4793970362644));
#30527=CARTESIAN_POINT('Ctrl Pts',(-23.8101198885386,26.7625090900617,-24.4791404212831));
#30528=CARTESIAN_POINT('Ctrl Pts',(-23.8124948036043,26.7623160788299,-24.4789928057272));
#30529=CARTESIAN_POINT('Ctrl Pts',(-23.8195179552625,26.7617374606436,-24.4785566731242));
#30530=CARTESIAN_POINT('Ctrl Pts',(-23.8241655967816,26.7613443943819,-24.4782685754838));
#30531=CARTESIAN_POINT('Ctrl Pts',(-23.8649685290172,26.7578043253812,-24.4757437032973));
#30532=CARTESIAN_POINT('Ctrl Pts',(-23.9010709602227,26.7540567345328,-24.4735401528992));
#30533=CARTESIAN_POINT('Ctrl Pts',(-24.0850469088672,26.7318118287296,-24.4624316296644));
#30534=CARTESIAN_POINT('Ctrl Pts',(-24.2315888290129,26.7036817315449,-24.4539779292751));
#30535=CARTESIAN_POINT('Ctrl Pts',(-24.6727856904948,26.5867819606826,-24.4283674860072));
#30536=CARTESIAN_POINT('Ctrl Pts',(-24.9570698253272,26.4659750863626,-24.4114705710625));
#30537=CARTESIAN_POINT('Ctrl Pts',(-25.2408271966982,26.2940949345589,-24.3914493253635));
#30538=CARTESIAN_POINT('Ctrl Pts',(-25.2615680613305,26.2812071151483,-24.3899672347442));
#30539=CARTESIAN_POINT('Ctrl Pts',(-25.2875883956991,26.2646259568132,-24.3880834199653));
#30540=CARTESIAN_POINT('Ctrl Pts',(-25.2930063466631,26.2611505627554,-24.3876898176084));
#30541=CARTESIAN_POINT('Ctrl Pts',(-25.3016051047201,26.2555983797952,-24.3870629637952));
#30542=CARTESIAN_POINT('Ctrl Pts',(-25.3047927341906,26.2535321455169,-24.3868301071897));
#30543=CARTESIAN_POINT('Ctrl Pts',(-25.3107854499251,26.2496325782911,-24.38639143699));
#30544=CARTESIAN_POINT('Ctrl Pts',(-25.3135913467412,26.2478004951887,-24.3861856704558));
#30545=CARTESIAN_POINT('Ctrl Pts',(-25.3198864802833,26.2436761299926,-24.3857231837511));
#30546=CARTESIAN_POINT('Ctrl Pts',(-25.3233741257845,26.2413814405684,-24.3854663733113));
#30547=CARTESIAN_POINT('Ctrl Pts',(-25.3322207599491,26.2355361520196,-24.3848134706495));
#30548=CARTESIAN_POINT('Ctrl Pts',(-25.3375735834468,26.2319762954514,-24.3844170298212));
#30549=CARTESIAN_POINT('Ctrl Pts',(-25.3670114078132,26.2122715948748,-24.382229090642));
#30550=CARTESIAN_POINT('Ctrl Pts',(-25.3908876964281,26.1958187108771,-24.3804259489078));
#30551=CARTESIAN_POINT('Ctrl Pts',(-25.420547413654,26.1747846595952,-24.3781491998147));
#30552=CARTESIAN_POINT('Ctrl Pts',(-25.4265420342252,26.170502431438,-24.3776871251509));
#30553=CARTESIAN_POINT('Ctrl Pts',(-25.4379895582557,26.162265520645,-24.3768010469268));
#30554=CARTESIAN_POINT('Ctrl Pts',(-25.4434448555878,26.158314217993,-24.3763771745035));
#30555=CARTESIAN_POINT('Ctrl Pts',(-25.4506736422669,26.153043735412,-24.3758133496465));
#30556=CARTESIAN_POINT('Ctrl Pts',(-25.4524582489989,26.1517397710777,-24.3756739803957));
#30557=CARTESIAN_POINT('Ctrl Pts',(-25.4584959367463,26.1473186600229,-24.3752018724596));
#30558=CARTESIAN_POINT('Ctrl Pts',(-25.4627426913871,26.1441929235276,-24.374868805511));
#30559=CARTESIAN_POINT('Ctrl Pts',(-25.4789472584008,26.1322044582896,-24.3735940742485));
#30560=CARTESIAN_POINT('Ctrl Pts',(-25.4908511484174,26.1232694568167,-24.3726496569076));
#30561=CARTESIAN_POINT('Ctrl Pts',(-25.5466781651561,26.0807581829191,-24.3681824733048));
#30562=CARTESIAN_POINT('Ctrl Pts',(-25.5897923591412,26.0461393228307,-24.3646203905203));
#30563=CARTESIAN_POINT('Ctrl Pts',(-25.7922967131517,25.8747852472769,-24.3473423809893));
#30564=CARTESIAN_POINT('Ctrl Pts',(-25.9389431022739,25.723810072234,-24.3331035367328));
#30565=CARTESIAN_POINT('Ctrl Pts',(-26.1793091158038,25.4224169657331,-24.3070379786952));
#30566=CARTESIAN_POINT('Ctrl Pts',(-26.2773881017931,25.276429187255,-24.2952556664628));
#30567=CARTESIAN_POINT('Ctrl Pts',(-26.3690376809031,25.1125316842191,-24.2834169688822));
#30568=CARTESIAN_POINT('Ctrl Pts',(-26.3749211754069,25.1018687639936,-24.2826527823063));
#30569=CARTESIAN_POINT('Ctrl Pts',(-26.3823816985277,25.0881646467886,-24.2816785826214));
#30570=CARTESIAN_POINT('Ctrl Pts',(-26.3840144138419,25.0851541203736,-24.2814650587251));
#30571=CARTESIAN_POINT('Ctrl Pts',(-26.3866303491642,25.0803122558447,-24.2811224375034));
#30572=CARTESIAN_POINT('Ctrl Pts',(-26.3876165961152,25.0784825696448,-24.2809931461232));
#30573=CARTESIAN_POINT('Ctrl Pts',(-26.3894908597987,25.0749973654298,-24.2807472175548));
#30574=CARTESIAN_POINT('Ctrl Pts',(-26.3903791925085,25.0733420373796,-24.280630560662));
#30575=CARTESIAN_POINT('Ctrl Pts',(-26.3923975312072,25.0695731391579,-24.2803652904408));
#30576=CARTESIAN_POINT('Ctrl Pts',(-26.3935266257324,25.0674590874345,-24.2802167360947));
#30577=CARTESIAN_POINT('Ctrl Pts',(-26.397023599987,25.0608939405748,-24.2797561451968));
#30578=CARTESIAN_POINT('Ctrl Pts',(-26.3993834083641,25.0564385195183,-24.2794446232843));
#30579=CARTESIAN_POINT('Ctrl Pts',(-26.4171602356189,25.022683823262,-24.2770923519426));
#30580=CARTESIAN_POINT('Ctrl Pts',(-26.4321361119596,24.9931527117092,-24.2750790808188));
#30581=CARTESIAN_POINT('Ctrl Pts',(-26.579979590395,24.6901299695189,-24.2548187603384));
#30582=CARTESIAN_POINT('Ctrl Pts',(-26.6739828158323,24.3993323757024,-24.2385300908595));
#30583=CARTESIAN_POINT('Ctrl Pts',(-26.7554840368577,23.9282288769233,-24.2114155426187));
#30584=CARTESIAN_POINT('Ctrl Pts',(-26.7712071638657,23.7547343293672,-24.2013077227666));
#30585=CARTESIAN_POINT('Ctrl Pts',(-26.7729543698201,23.5706188576439,-24.1900992063219));
#30586=CARTESIAN_POINT('Ctrl Pts',(-26.7730027367683,23.5604032267184,-24.1894758147137));
#30587=CARTESIAN_POINT('Ctrl Pts',(-26.7730024481601,23.5460721172818,-24.1885991423379));
#30588=CARTESIAN_POINT('Ctrl Pts',(-26.7729944818974,23.5419566236212,-24.1883471389412));
#30589=CARTESIAN_POINT('Ctrl Pts',(-26.7729654429978,23.5344164006638,-24.1878849716837));
#30590=CARTESIAN_POINT('Ctrl Pts',(-26.7729467943467,23.5309916631083,-24.1876748841723));
#30591=CARTESIAN_POINT('Ctrl Pts',(-26.7728980092678,23.5240613418659,-24.1872493968364));
#30592=CARTESIAN_POINT('Ctrl Pts',(-26.7728676117933,23.5205557656606,-24.1870339891313));
#30593=CARTESIAN_POINT('Ctrl Pts',(-26.7727788835205,23.5119438898649,-24.1865043616412));
#30594=CARTESIAN_POINT('Ctrl Pts',(-26.7727141358576,23.5068376786332,-24.1861899407832));
#30595=CARTESIAN_POINT('Ctrl Pts',(-26.77243530426,23.4883198168534,-24.1850482512166));
#30596=CARTESIAN_POINT('Ctrl Pts',(-26.7721496286861,23.4749095251215,-24.1842187379668));
#30597=CARTESIAN_POINT('Ctrl Pts',(-26.766790052078,23.2803648806809,-24.1721444470134));
#30598=CARTESIAN_POINT('Ctrl Pts',(-26.7465330965104,23.1000046048152,-24.1604131008969));
#30599=CARTESIAN_POINT('Ctrl Pts',(-26.6505728266991,22.6169393471348,-24.1275965740543));
#30600=CARTESIAN_POINT('Ctrl Pts',(-26.5459786080223,22.3219673449654,-24.1058982575636));
#30601=CARTESIAN_POINT('Ctrl Pts',(-26.3932673462726,22.0324783221359,-24.0851894584158));
#30602=CARTESIAN_POINT('Ctrl Pts',(-26.385723253345,22.0184308714549,-24.0841866006848));
#30603=CARTESIAN_POINT('Ctrl Pts',(-26.3763650867354,22.0013115717109,-24.0829674816765));
#30604=CARTESIAN_POINT('Ctrl Pts',(-26.3746499423254,21.9981863158393,-24.0827450471344));
#30605=CARTESIAN_POINT('Ctrl Pts',(-26.3718107114501,21.9930330940964,-24.0823784899465));
#30606=CARTESIAN_POINT('Ctrl Pts',(-26.3706896220525,21.9910034951441,-24.0822341761736));
#30607=CARTESIAN_POINT('Ctrl Pts',(-26.3686620880612,21.9873422274789,-24.0819739450208));
#30608=CARTESIAN_POINT('Ctrl Pts',(-26.3677564186201,21.9857101405592,-24.0818579782231));
#30609=CARTESIAN_POINT('Ctrl Pts',(-26.3658033691769,21.9821977889061,-24.081608489898));
#30610=CARTESIAN_POINT('Ctrl Pts',(-26.3647555262799,21.9803177915336,-24.0814749992009));
#30611=CARTESIAN_POINT('Ctrl Pts',(-26.3618744257787,21.9751607925527,-24.0811089522741));
#30612=CARTESIAN_POINT('Ctrl Pts',(-26.3600373157019,21.9718859298215,-24.0808766446092));
#30613=CARTESIAN_POINT('Ctrl Pts',(-26.3503791746485,21.954739468497,-24.0796610486636));
#30614=CARTESIAN_POINT('Ctrl Pts',(-26.342460952926,21.9409224510512,-24.0786839524006));
#30615=CARTESIAN_POINT('Ctrl Pts',(-26.2425535918111,21.7695449051666,-24.0665881839196));
#30616=CARTESIAN_POINT('Ctrl Pts',(-26.1374328324067,21.6199875102982,-24.0562719498195));
#30617=CARTESIAN_POINT('Ctrl Pts',(-25.8787942388071,21.3113972672536,-24.0337156542308));
#30618=CARTESIAN_POINT('Ctrl Pts',(-25.7204834332987,21.1576242166834,-24.0215484534736));
#30619=CARTESIAN_POINT('Ctrl Pts',(-25.4736594461816,20.962679400865,-24.0032057382177));
#30620=CARTESIAN_POINT('Ctrl Pts',(-25.3970504099156,20.9074578362577,-23.997594077638));
#30621=CARTESIAN_POINT('Ctrl Pts',(-25.309547620996,20.8500481308872,-23.9912234706796));
#30622=CARTESIAN_POINT('Ctrl Pts',(-25.300934715666,20.8444559938398,-23.9905968397905));
#30623=CARTESIAN_POINT('Ctrl Pts',(-25.2888254725746,20.8366757957987,-23.9897163776854));
#30624=CARTESIAN_POINT('Ctrl Pts',(-25.2853513739022,20.8344530950889,-23.9894638387473));
#30625=CARTESIAN_POINT('Ctrl Pts',(-25.2789826769736,20.830395661883,-23.9890009958823));
#30626=CARTESIAN_POINT('Ctrl Pts',(-25.2760893962197,20.8285588633392,-23.9887907691329));
#30627=CARTESIAN_POINT('Ctrl Pts',(-25.2702328803411,20.8248539492092,-23.9883653138106));
#30628=CARTESIAN_POINT('Ctrl Pts',(-25.2672695191249,20.8229860434568,-23.9881500778712));
#30629=CARTESIAN_POINT('Ctrl Pts',(-25.2599899739694,20.8184140696937,-23.9876214465936));
#30630=CARTESIAN_POINT('Ctrl Pts',(-25.2556704244734,20.8157154018502,-23.9873078518885));
#30631=CARTESIAN_POINT('Ctrl Pts',(-25.2402792684196,20.8061503251487,-23.9861907599558));
#30632=CARTESIAN_POINT('Ctrl Pts',(-25.2291725577093,20.7993408956997,-23.9853851647965));
#30633=CARTESIAN_POINT('Ctrl Pts',(-25.0768004289212,20.7071893456473,-23.9743396876003));
#30634=CARTESIAN_POINT('Ctrl Pts',(-24.9292473700157,20.6327682584562,-23.9636990083846));
#30635=CARTESIAN_POINT('Ctrl Pts',(-24.5119950272348,20.461064647255,-23.9337742698664));
#30636=CARTESIAN_POINT('Ctrl Pts',(-24.2340204520156,20.3878992887072,-23.9139196522787));
#30637=CARTESIAN_POINT('Ctrl Pts',(-23.9470354765121,20.3520201929175,-23.8951205970291));
#30638=CARTESIAN_POINT('Ctrl Pts',(-23.9440193939772,20.3516474519105,-23.8949232288537));
#30639=CARTESIAN_POINT('Ctrl Pts',(-23.9323667444999,20.350224096708,-23.8941614849061));
#30640=CARTESIAN_POINT('Ctrl Pts',(-23.9237263824441,20.3492041811732,-23.8935983304071));
#30641=CARTESIAN_POINT('Ctrl Pts',(-23.9134437259337,20.3480326083604,-23.8929302063955));
#30642=CARTESIAN_POINT('Ctrl Pts',(-23.9118054007822,20.3478472163345,-23.8928238173666));
#30643=CARTESIAN_POINT('Ctrl Pts',(-23.9074597642698,20.3473588436667,-23.8925417887819));
#30644=CARTESIAN_POINT('Ctrl Pts',(-23.9047522037392,20.3470580376876,-23.8923662419409));
#30645=CARTESIAN_POINT('Ctrl Pts',(-23.8630352829491,20.3424768905867,-23.8896641713945));
#30646=CARTESIAN_POINT('Ctrl Pts',(-23.8239490751474,20.3389057483981,-23.8871685558398));
#30647=CARTESIAN_POINT('Ctrl Pts',(-23.7800477678339,20.3357021018247,-23.8844131272201));
#30648=CARTESIAN_POINT('Ctrl Pts',(-23.7752894778093,20.3353654900852,-23.8841151038464));
#30649=CARTESIAN_POINT('Ctrl Pts',(-23.7681262491319,20.3348747291761,-23.8836674143066));
#30650=CARTESIAN_POINT('Ctrl Pts',(-23.7657218828922,20.3347127125559,-23.8835173084496));
#30651=CARTESIAN_POINT('Ctrl Pts',(-23.7615590213966,20.3344368909703,-23.8832577034981));
#30652=CARTESIAN_POINT('Ctrl Pts',(-23.7598006148731,20.3343218314792,-23.8831481334284));
#30653=CARTESIAN_POINT('Ctrl Pts',(-23.7561382798192,20.3340852069241,-23.8829201098612));
#30654=CARTESIAN_POINT('Ctrl Pts',(-23.7542343397835,20.3339638903894,-23.8828016710548));
#30655=CARTESIAN_POINT('Ctrl Pts',(-23.7497654691771,20.3336831239949,-23.882523916806));
#30656=CARTESIAN_POINT('Ctrl Pts',(-23.7472004462455,20.3335250508786,-23.8823646794655));
#30657=CARTESIAN_POINT('Ctrl Pts',(-23.7387871980561,20.3330166736344,-23.8818429873877));
#30658=CARTESIAN_POINT('Ctrl Pts',(-23.7329381626823,20.3326792460775,-23.8814812562427));
#30659=CARTESIAN_POINT('Ctrl Pts',(-23.7191303365629,20.3319204530977,-23.8806295099922));
#30660=CARTESIAN_POINT('Ctrl Pts',(-23.7111707959164,20.3315126545934,-23.8801402386767));
#30661=CARTESIAN_POINT('Ctrl Pts',(-23.4323053348698,20.3182622931688,-23.8630560864631));
#30662=CARTESIAN_POINT('Ctrl Pts',(-23.16080701125,20.3396357480102,-23.8482691213606));
#30663=CARTESIAN_POINT('Ctrl Pts',(-22.7479223309423,20.4253530435576,-23.8246348929832));
#30664=CARTESIAN_POINT('Ctrl Pts',(-22.6030162188156,20.4661857497469,-23.8161204641292));
#30665=CARTESIAN_POINT('Ctrl Pts',(-22.4480413576374,20.5218119157592,-23.8064594158265));
#30666=CARTESIAN_POINT('Ctrl Pts',(-22.4346150897375,20.5267322116466,-23.8056178439904));
#30667=CARTESIAN_POINT('Ctrl Pts',(-22.4148446274654,20.5341270673599,-23.8043715685224));
#30668=CARTESIAN_POINT('Ctrl Pts',(-22.408474710319,20.536532682202,-23.8039689420992));
#30669=CARTESIAN_POINT('Ctrl Pts',(-22.3983656136364,20.5403870578628,-23.803328218135));
#30670=CARTESIAN_POINT('Ctrl Pts',(-22.3946214105764,20.5418226498031,-23.8030905238647));
#30671=CARTESIAN_POINT('Ctrl Pts',(-22.3861982872293,20.5450702653078,-23.8025549251685));
#30672=CARTESIAN_POINT('Ctrl Pts',(-22.381520906744,20.5468862325729,-23.8022568995735));
#30673=CARTESIAN_POINT('Ctrl Pts',(-22.3703978204451,20.5512346285788,-23.8015467164951));
#30674=CARTESIAN_POINT('Ctrl Pts',(-22.3639560170771,20.5537769183789,-23.8011342522416));
#30675=CARTESIAN_POINT('Ctrl Pts',(-22.3556000050665,20.557105828695,-23.8005976785059));
#30676=CARTESIAN_POINT('Ctrl Pts',(-22.353678257408,20.5578735698746,-23.8004741689376));
#30677=CARTESIAN_POINT('Ctrl Pts',(-22.3476820297402,20.5602757720516,-23.8000884617111));
#30678=CARTESIAN_POINT('Ctrl Pts',(-22.3436101607425,20.5619167032242,-23.7998260581191));
#30679=CARTESIAN_POINT('Ctrl Pts',(-22.3381046787364,20.5641484562573,-23.7994706115027));
#30680=CARTESIAN_POINT('Ctrl Pts',(-22.3366681078595,20.5647320053899,-23.7993778025879));
#30681=CARTESIAN_POINT('Ctrl Pts',(-22.331470850864,20.5668475530221,-23.7990418165322));
#30682=CARTESIAN_POINT('Ctrl Pts',(-22.3277126509722,20.5683856178107,-23.7987984439021));
#30683=CARTESIAN_POINT('Ctrl Pts',(-22.3142021397951,20.5739447069637,-23.7979220204694));
#30684=CARTESIAN_POINT('Ctrl Pts',(-22.3044667538371,20.5780064734786,-23.7972876482053));
#30685=CARTESIAN_POINT('Ctrl Pts',(-22.2709709904118,20.5921749464184,-23.7950950191172));
#30686=CARTESIAN_POINT('Ctrl Pts',(-22.2473127128763,20.6025191599446,-23.7935289351613));
#30687=CARTESIAN_POINT('Ctrl Pts',(-22.2176177406058,20.6159301530916,-23.7915402977232));
#30688=CARTESIAN_POINT('Ctrl Pts',(-22.2114624926143,20.6187333797618,-23.7911268341268));
#30689=CARTESIAN_POINT('Ctrl Pts',(-22.2017611015577,20.6231885199193,-23.7904731684279));
#30690=CARTESIAN_POINT('Ctrl Pts',(-22.1982090397507,20.6248275605389,-23.7902334114089));
#30691=CARTESIAN_POINT('Ctrl Pts',(-22.1916569267781,20.6278654078197,-23.7897903695151));
#30692=CARTESIAN_POINT('Ctrl Pts',(-22.1886560260014,20.629262378503,-23.789587148441));
#30693=CARTESIAN_POINT('Ctrl Pts',(-22.1820206347767,20.6323637138716,-23.7891371202448));
#30694=CARTESIAN_POINT('Ctrl Pts',(-22.1783871700797,20.6340702489337,-23.7888902380685));
#30695=CARTESIAN_POINT('Ctrl Pts',(-22.1681836681901,20.6388858336101,-23.7881956664484));
#30696=CARTESIAN_POINT('Ctrl Pts',(-22.1616209776259,20.6420103134738,-23.7877474411647));
#30697=CARTESIAN_POINT('Ctrl Pts',(-22.1219007421649,20.6610861127146,-23.7850254711747));
#30698=CARTESIAN_POINT('Ctrl Pts',(-22.0890089303692,20.6775815815664,-23.7827327932335));
#30699=CARTESIAN_POINT('Ctrl Pts',(-21.9932549035333,20.727672918416,-23.775940772644));
#30700=CARTESIAN_POINT('Ctrl Pts',(-21.931219655381,20.7627933742059,-23.7713883736102));
#30701=CARTESIAN_POINT('Ctrl Pts',(-21.7501365379864,20.8733961698955,-23.757634152848));
#30702=CARTESIAN_POINT('Ctrl Pts',(-21.6348297273714,20.9546551705515,-23.7482446119146));
#30703=CARTESIAN_POINT('Ctrl Pts',(-21.3604613216403,21.1762710365889,-23.7244600478107));
#30704=CARTESIAN_POINT('Ctrl Pts',(-21.2092161194307,21.325273779263,-23.7099592694294));
#30705=CARTESIAN_POINT('Ctrl Pts',(-21.0691689069866,21.493461026055,-23.6957428109769));
#30706=CARTESIAN_POINT('Ctrl Pts',(-21.0646760818302,21.4988927475438,-23.695285834948));
#30707=CARTESIAN_POINT('Ctrl Pts',(-21.0555852536157,21.5099570628334,-23.69435942076));
#30708=CARTESIAN_POINT('Ctrl Pts',(-21.0509884134667,21.515590570128,-23.6938900453711));
#30709=CARTESIAN_POINT('Ctrl Pts',(-21.0421924103202,21.5264450113449,-23.6929901874747));
#30710=CARTESIAN_POINT('Ctrl Pts',(-21.0379903899416,21.5316635729054,-23.6925595477772));
#30711=CARTESIAN_POINT('Ctrl Pts',(-21.012864403665,21.5630679519031,-23.6899801450836));
#30712=CARTESIAN_POINT('Ctrl Pts',(-20.9923327208649,21.5895670576824,-23.6878539924824));
#30713=CARTESIAN_POINT('Ctrl Pts',(-20.9691807075941,21.6204309316236,-23.6854395457123));
#30714=CARTESIAN_POINT('Ctrl Pts',(-20.9661536889331,21.6244861022082,-23.6851235257715));
#30715=CARTESIAN_POINT('Ctrl Pts',(-20.9617049419742,21.6304752791011,-23.6846585925624));
#30716=CARTESIAN_POINT('Ctrl Pts',(-20.9602758217878,21.6324037456707,-23.6845091626482));
#30717=CARTESIAN_POINT('Ctrl Pts',(-20.957731722874,21.6358448035968,-23.6842430197704));
#30718=CARTESIAN_POINT('Ctrl Pts',(-20.9566159126651,21.6373567734085,-23.6841262481696));
#30719=CARTESIAN_POINT('Ctrl Pts',(-20.9542697997638,21.6405416817682,-23.6838806299165));
#30720=CARTESIAN_POINT('Ctrl Pts',(-20.9530397944163,21.6422148297119,-23.6837518042901));
#30721=CARTESIAN_POINT('Ctrl Pts',(-20.9498312060558,21.6465882498758,-23.6834156044054));
#30722=CARTESIAN_POINT('Ctrl Pts',(-20.9478552051094,21.649290426987,-23.6832084113911));
#30723=CARTESIAN_POINT('Ctrl Pts',(-20.9391556064585,21.6612260964148,-23.682295551724));
#30724=CARTESIAN_POINT('Ctrl Pts',(-20.9324768054736,21.6704923654461,-23.6815929764616));
#30725=CARTESIAN_POINT('Ctrl Pts',(-20.7648079871324,21.9057453495876,-23.6639047990543));
#30726=CARTESIAN_POINT('Ctrl Pts',(-20.6335913016358,22.1515919264555,-23.6488142119931));
#30727=CARTESIAN_POINT('Ctrl Pts',(-20.4929026413639,22.5239732263405,-23.6264859908256));
#30728=CARTESIAN_POINT('Ctrl Pts',(-20.4566731781995,22.6389889467513,-23.6196667255412));
#30729=CARTESIAN_POINT('Ctrl Pts',(-20.4213715694493,22.7777648678965,-23.611349375747));
#30730=CARTESIAN_POINT('Ctrl Pts',(-20.4160060215637,22.7998312850777,-23.6100243919422));
#30731=CARTESIAN_POINT('Ctrl Pts',(-20.406786065273,22.8395744107522,-23.6076322084003));
#30732=CARTESIAN_POINT('Ctrl Pts',(-20.4028464228304,22.8572304648466,-23.6065674294376));
#30733=CARTESIAN_POINT('Ctrl Pts',(-20.3980831448805,22.8794565426786,-23.6052240434625));
#30734=CARTESIAN_POINT('Ctrl Pts',(-20.3971204060971,22.8839966497238,-23.6049494739503));
#30735=CARTESIAN_POINT('Ctrl Pts',(-20.3953438417585,22.892464714974,-23.6044370526568));
#30736=CARTESIAN_POINT('Ctrl Pts',(-20.3945275355068,22.8963921475972,-23.6041992737519));
#30737=CARTESIAN_POINT('Ctrl Pts',(-20.3927231901507,22.9051553447019,-23.6036684443759));
#30738=CARTESIAN_POINT('Ctrl Pts',(-20.3917389245447,22.9099918688072,-23.6033752837712));
#30739=CARTESIAN_POINT('Ctrl Pts',(-20.3893980467729,22.9216313356403,-23.6026693006691));
#30740=CARTESIAN_POINT('Ctrl Pts',(-20.3880522852024,22.9284364150007,-23.6022561582308));
#30741=CARTESIAN_POINT('Ctrl Pts',(-20.386356173301,22.9371610191565,-23.6017259640447));
#30742=CARTESIAN_POINT('Ctrl Pts',(-20.3859855739064,22.9390766247513,-23.6016095208772));
#30743=CARTESIAN_POINT('Ctrl Pts',(-20.3845509011245,22.9465286437605,-23.6011564127289));
#30744=CARTESIAN_POINT('Ctrl Pts',(-20.3834996210228,22.9520674860645,-23.6008193635447));
#30745=CARTESIAN_POINT('Ctrl Pts',(-20.3818845289956,22.9607004531195,-23.6002935988242));
#30746=CARTESIAN_POINT('Ctrl Pts',(-20.3813107001516,22.9637927103325,-23.6001051879877));
#30747=CARTESIAN_POINT('Ctrl Pts',(-20.3791000905458,22.9758032541401,-23.5993730464057));
#30748=CARTESIAN_POINT('Ctrl Pts',(-20.3774964349613,22.9847275317053,-23.5988283089596));
#30749=CARTESIAN_POINT('Ctrl Pts',(-20.371047878187,23.021504411815,-23.5965803086276));
#30750=CARTESIAN_POINT('Ctrl Pts',(-20.3665320274462,23.049412761456,-23.5948669746406));
#30751=CARTESIAN_POINT('Ctrl Pts',(-20.3614494646558,23.0836765682424,-23.5927532826252));
#30752=CARTESIAN_POINT('Ctrl Pts',(-20.360533583047,23.0899796151041,-23.592364035024));
#30753=CARTESIAN_POINT('Ctrl Pts',(-20.3590509169601,23.1004002314163,-23.5917197957695));
#30754=CARTESIAN_POINT('Ctrl Pts',(-20.3584733995894,23.1045162761006,-23.5914651446945));
#30755=CARTESIAN_POINT('Ctrl Pts',(-20.3574448583731,23.1119513305294,-23.5910048193579));
#30756=CARTESIAN_POINT('Ctrl Pts',(-20.3569910425335,23.1152699533436,-23.5907992338866));
#30757=CARTESIAN_POINT('Ctrl Pts',(-20.3560318986578,23.1223662892296,-23.5903593634743));
#30758=CARTESIAN_POINT('Ctrl Pts',(-20.3555280972335,23.1261442004075,-23.5901250305081));
#30759=CARTESIAN_POINT('Ctrl Pts',(-20.3542010158115,23.1362322828458,-23.5894988722143));
#30760=CARTESIAN_POINT('Ctrl Pts',(-20.3533897253129,23.1425439901125,-23.5891066679494));
#30761=CARTESIAN_POINT('Ctrl Pts',(-20.3495813288464,23.1728830685771,-23.5872192627774));
#30762=CARTESIAN_POINT('Ctrl Pts',(-20.3468364451308,23.196940792269,-23.5857161086511));
#30763=CARTESIAN_POINT('Ctrl Pts',(-20.3331476443629,23.3302376721122,-23.5773496685747));
#30764=CARTESIAN_POINT('Ctrl Pts',(-20.3275213050042,23.4399384600812,-23.5703199306854));
#30765=CARTESIAN_POINT('Ctrl Pts',(-20.3274657168425,23.7657667085965,-23.5490035681645));
#30766=CARTESIAN_POINT('Ctrl Pts',(-20.349157902338,23.9812695237662,-23.5342952087362));
#30767=CARTESIAN_POINT('Ctrl Pts',(-20.4242855499426,24.3504227763822,-23.5088742976067));
#30768=CARTESIAN_POINT('Ctrl Pts',(-20.4680713323199,24.5052996682065,-23.4981541099756));
#30769=CARTESIAN_POINT('Ctrl Pts',(-20.5264718386568,24.6651322124755,-23.4874519413867));
#30770=CARTESIAN_POINT('Ctrl Pts',(-20.529745103123,24.6739701392045,-23.4868614022524));
#30771=CARTESIAN_POINT('Ctrl Pts',(-20.5341928331809,24.6858193071609,-23.4860714414125));
#30772=CARTESIAN_POINT('Ctrl Pts',(-20.5353330843489,24.6888432100233,-23.4858700003323));
#30773=CARTESIAN_POINT('Ctrl Pts',(-20.5371268904546,24.6935787271738,-23.4855547892503));
#30774=CARTESIAN_POINT('Ctrl Pts',(-20.5377773556571,24.695291497392,-23.4854408333968));
#30775=CARTESIAN_POINT('Ctrl Pts',(-20.5390295541023,24.69858026695,-23.4852221218783));
#30776=CARTESIAN_POINT('Ctrl Pts',(-20.5396310602909,24.7001563382259,-23.4851173536515));
#30777=CARTESIAN_POINT('Ctrl Pts',(-20.5410586083286,24.7038880126808,-23.4848693978276));
#30778=CARTESIAN_POINT('Ctrl Pts',(-20.5418857280567,24.7060431988409,-23.4847262763112));
#30779=CARTESIAN_POINT('Ctrl Pts',(-20.5442921572474,24.7122934317031,-23.484311445562));
#30780=CARTESIAN_POINT('Ctrl Pts',(-20.5458775253894,24.716386163861,-23.4840401013514));
#30781=CARTESIAN_POINT('Ctrl Pts',(-20.5574004510024,24.745953879614,-23.482081816879));
#30782=CARTESIAN_POINT('Ctrl Pts',(-20.5676539074737,24.7713057071099,-23.4804136411855));
#30783=CARTESIAN_POINT('Ctrl Pts',(-20.6007665205555,24.8502703506694,-23.4752427358927));
#30784=CARTESIAN_POINT('Ctrl Pts',(-20.6247590735966,24.903398119426,-23.4718001964935));
#30785=CARTESIAN_POINT('Ctrl Pts',(-20.7324588542617,25.1256077120508,-23.45743864668));
#30786=CARTESIAN_POINT('Ctrl Pts',(-20.8294895028433,25.2878269320418,-23.4470296570714));
#30787=CARTESIAN_POINT('Ctrl Pts',(-21.0754982611935,25.6274963677508,-23.4235442770395));
#30788=CARTESIAN_POINT('Ctrl Pts',(-21.2304849904737,25.7992536462733,-23.4104254281309));
#30789=CARTESIAN_POINT('Ctrl Pts',(-21.4135859341381,25.9629265584005,-23.3955241237047));
#30790=CARTESIAN_POINT('Ctrl Pts',(-21.4247768227455,25.9727910984094,-23.3946157782963));
#30791=CARTESIAN_POINT('Ctrl Pts',(-21.4401940093273,25.98619197087,-23.3933674926352));
#30792=CARTESIAN_POINT('Ctrl Pts',(-21.4443616089297,25.9897957963171,-23.3930303611992));
#30793=CARTESIAN_POINT('Ctrl Pts',(-21.4509892080793,25.9954972049312,-23.3924947093769));
#30794=CARTESIAN_POINT('Ctrl Pts',(-21.4534431707852,25.9976018156644,-23.3922964800495));
#30795=CARTESIAN_POINT('Ctrl Pts',(-21.458207405974,26.0016753774308,-23.391911826622));
#30796=CARTESIAN_POINT('Ctrl Pts',(-21.4605173026228,26.003644764691,-23.3917254207921));
#30797=CARTESIAN_POINT('Ctrl Pts',(-21.4660234693189,26.0083258315441,-23.3912812916404));
#30798=CARTESIAN_POINT('Ctrl Pts',(-21.4692222480699,26.0110345395645,-23.3910234465167));
#30799=CARTESIAN_POINT('Ctrl Pts',(-21.4758587811278,26.0166321241154,-23.3904888387139));
#30800=CARTESIAN_POINT('Ctrl Pts',(-21.4792973052858,26.0195200700919,-23.3902120386211));
#30801=CARTESIAN_POINT('Ctrl Pts',(-21.498944167284,26.0359511626844,-23.3886315461787));
#30802=CARTESIAN_POINT('Ctrl Pts',(-21.5152789949966,26.0493416378965,-23.387321642926));
#30803=CARTESIAN_POINT('Ctrl Pts',(-21.5584549584209,26.0840311395242,-23.3838695119901));
#30804=CARTESIAN_POINT('Ctrl Pts',(-21.5855056430197,26.1050638992508,-23.3817167949403));
#30805=CARTESIAN_POINT('Ctrl Pts',(-21.7092023617559,26.1981155243112,-23.3719151217746));
#30806=CARTESIAN_POINT('Ctrl Pts',(-21.8094967939359,26.2651020372075,-23.3640769187142));
#30807=CARTESIAN_POINT('Ctrl Pts',(-21.9663631470339,26.3576013138764,-23.351998894681));
#30808=CARTESIAN_POINT('Ctrl Pts',(-22.0202990286664,26.3873549640467,-23.347877474289));
#30809=CARTESIAN_POINT('Ctrl Pts',(-22.0750361484425,26.4155368430821,-23.3437344129902));
#30810=CARTESIAN_POINT('Origin',(-23.5502525316942,23.5502525316942,-77.3107734492734));
#30811=CARTESIAN_POINT('',(-22.0750357083693,26.4155366165066,-21.8446295278275));
#30812=CARTESIAN_POINT('',(-22.0750360154714,26.4155367746208,-22.0897962101869));
#30813=CARTESIAN_POINT('',(-22.0750360153461,26.4155367745563,-77.3107734492734));
#30814=CARTESIAN_POINT('Ctrl Pts',(-22.0750357083693,26.4155366165066,-21.8446295278275));
#30815=CARTESIAN_POINT('Ctrl Pts',(-22.0175648871972,26.3859472565221,-21.8489280757192));
#30816=CARTESIAN_POINT('Ctrl Pts',(-21.9609748464247,26.3546239485576,-21.8532666299503));
#30817=CARTESIAN_POINT('Ctrl Pts',(-21.7998026708723,26.2589618161571,-21.8659034386297));
#30818=CARTESIAN_POINT('Ctrl Pts',(-21.6979264287397,26.1903412992165,-21.8742489937229));
#30819=CARTESIAN_POINT('Ctrl Pts',(-21.5244223507677,26.0584773150897,-21.8888979493505));
#30820=CARTESIAN_POINT('Ctrl Pts',(-21.4512157560001,25.9975422367158,-21.8952310941675));
#30821=CARTESIAN_POINT('Ctrl Pts',(-21.3558308332747,25.9107126436346,-21.9035866384558));
#30822=CARTESIAN_POINT('Ctrl Pts',(-21.3312099826078,25.8875819698615,-21.9057532493313));
#30823=CARTESIAN_POINT('Ctrl Pts',(-21.2941318082051,25.8516338354809,-21.9090251984061));
#30824=CARTESIAN_POINT('Ctrl Pts',(-21.2814105753201,25.8390934690216,-21.9101494660534));
#30825=CARTESIAN_POINT('Ctrl Pts',(-21.2660424491475,25.8236898054178,-21.9115089783301));
#30826=CARTESIAN_POINT('Ctrl Pts',(-21.2632959612886,25.8209269654747,-21.9117519931002));
#30827=CARTESIAN_POINT('Ctrl Pts',(-21.2590180584144,25.8166079578517,-21.9121305815918));
#30828=CARTESIAN_POINT('Ctrl Pts',(-21.2574832153539,25.8150552143436,-21.9122664274059));
#30829=CARTESIAN_POINT('Ctrl Pts',(-21.2547721363206,25.8123069363795,-21.9125064027904));
#30830=CARTESIAN_POINT('Ctrl Pts',(-21.2535952618458,25.8111120497052,-21.9126105833104));
#30831=CARTESIAN_POINT('Ctrl Pts',(-21.2510818220564,25.8085561536955,-21.9128330972335));
#30832=CARTESIAN_POINT('Ctrl Pts',(-21.2497455360575,25.8071948801547,-21.9129514083752));
#30833=CARTESIAN_POINT('Ctrl Pts',(-21.2458864310717,25.803256624501,-21.9132931155375));
#30834=CARTESIAN_POINT('Ctrl Pts',(-21.2433667176426,25.8006765826526,-21.9135162655098));
#30835=CARTESIAN_POINT('Ctrl Pts',(-21.2321827625733,25.7891863333612,-21.9145069439859));
#30836=CARTESIAN_POINT('Ctrl Pts',(-21.2235656232407,25.7802301245495,-21.9152708122574));
#30837=CARTESIAN_POINT('Ctrl Pts',(-21.213063906329,25.7691880394058,-21.9162027683702));
#30838=CARTESIAN_POINT('Ctrl Pts',(-21.2111301221775,25.7671494195417,-21.9163744217491));
#30839=CARTESIAN_POINT('Ctrl Pts',(-21.0368363059738,25.5829247099505,-21.9318498942574));
#30840=CARTESIAN_POINT('Ctrl Pts',(-20.8862975578017,25.3812101444086,-21.9456286065462));
#30841=CARTESIAN_POINT('Ctrl Pts',(-20.6817044623154,25.0275522702009,-21.9684852111726));
#30842=CARTESIAN_POINT('Ctrl Pts',(-20.6128721779985,24.8854578161312,-21.9773680046081));
#30843=CARTESIAN_POINT('Ctrl Pts',(-20.531997760293,24.6816458296823,-21.9901818120448));
#30844=CARTESIAN_POINT('Ctrl Pts',(-20.5109237958273,24.6237481151354,-21.9938278098427));
#30845=CARTESIAN_POINT('Ctrl Pts',(-20.4847155180432,24.5447712697004,-21.998826647149));
#30846=CARTESIAN_POINT('Ctrl Pts',(-20.4781148537225,24.5241902890543,-22.0001315745631));
#30847=CARTESIAN_POINT('Ctrl Pts',(-20.4687890124242,24.4940737252635,-22.0020450068197));
#30848=CARTESIAN_POINT('Ctrl Pts',(-20.4658999503546,24.484589203659,-22.0026481592239));
#30849=CARTESIAN_POINT('Ctrl Pts',(-20.4607996145595,24.4675638137298,-22.0037319302085));
#30850=CARTESIAN_POINT('Ctrl Pts',(-20.4585720599139,24.4600278743091,-22.004212013445));
#30851=CARTESIAN_POINT('Ctrl Pts',(-20.4552276040109,24.4485592567871,-22.0049432252287));
#30852=CARTESIAN_POINT('Ctrl Pts',(-20.4540905757563,24.4446324384933,-22.0051936954517));
#30853=CARTESIAN_POINT('Ctrl Pts',(-20.4520501340863,24.4375350878176,-22.0056465913305));
#30854=CARTESIAN_POINT('Ctrl Pts',(-20.4511441066211,24.4343653075644,-22.0058489313075));
#30855=CARTESIAN_POINT('Ctrl Pts',(-20.4492091566527,24.4275562712909,-22.0062837326579));
#30856=CARTESIAN_POINT('Ctrl Pts',(-20.4481817740777,24.4239165860908,-22.0065162439245));
#30857=CARTESIAN_POINT('Ctrl Pts',(-20.4454432491164,24.4141491451834,-22.0071404654883));
#30858=CARTESIAN_POINT('Ctrl Pts',(-20.4437438482596,24.4080181400019,-22.0075325577168));
#30859=CARTESIAN_POINT('Ctrl Pts',(-20.4364320871533,24.3813324296251,-22.0092403753001));
#30860=CARTESIAN_POINT('Ctrl Pts',(-20.4310055984136,24.3607277575227,-22.010562128267));
#30861=CARTESIAN_POINT('Ctrl Pts',(-20.4225719059793,24.3273646466107,-22.0127077012763));
#30862=CARTESIAN_POINT('Ctrl Pts',(-20.4194374659943,24.3146387899524,-22.0135273558651));
#30863=CARTESIAN_POINT('Ctrl Pts',(-20.4152862838243,24.2973309808365,-22.0146438920765));
#30864=CARTESIAN_POINT('Ctrl Pts',(-20.4142017659447,24.2927652781992,-22.0149385942929));
#30865=CARTESIAN_POINT('Ctrl Pts',(-20.4124757908339,24.2854278718688,-22.0154124711553));
#30866=CARTESIAN_POINT('Ctrl Pts',(-20.4118280219748,24.282657647047,-22.0155914441848));
#30867=CARTESIAN_POINT('Ctrl Pts',(-20.3361989812132,23.9572825500086,-22.0366198922923));
#30868=CARTESIAN_POINT('Ctrl Pts',(-20.3114089338969,23.6250972393798,-22.0592364297752));
#30869=CARTESIAN_POINT('Ctrl Pts',(-20.3480106217355,23.1642630480681,-22.0903078671484));
#30870=CARTESIAN_POINT('Ctrl Pts',(-20.3663846149854,23.0341763322658,-22.0990027326934));
#30871=CARTESIAN_POINT('Ctrl Pts',(-20.3957324201398,22.8904353686377,-22.1082785590399));
#30872=CARTESIAN_POINT('Ctrl Pts',(-20.3989289333594,22.8753337038302,-22.1092488839153));
#30873=CARTESIAN_POINT('Ctrl Pts',(-20.4030295934696,22.8566250010155,-22.1104452450256));
#30874=CARTESIAN_POINT('Ctrl Pts',(-20.4038315680157,22.8529961270202,-22.1106770318504));
#30875=CARTESIAN_POINT('Ctrl Pts',(-20.4051060258887,22.8472762769086,-22.1110419439171));
#30876=CARTESIAN_POINT('Ctrl Pts',(-20.405574318107,22.8451843854648,-22.1111753102482));
#30877=CARTESIAN_POINT('Ctrl Pts',(-20.4064544359313,22.8412711621274,-22.1114246211755));
#30878=CARTESIAN_POINT('Ctrl Pts',(-20.40686575448,22.8394497333201,-22.1115405939494));
#30879=CARTESIAN_POINT('Ctrl Pts',(-20.4077939194577,22.8353561317143,-22.1118010819986));
#30880=CARTESIAN_POINT('Ctrl Pts',(-20.4083116462021,22.8330841661825,-22.1119455453993));
#30881=CARTESIAN_POINT('Ctrl Pts',(-20.4096360125962,22.827301344428,-22.1123129755955));
#30882=CARTESIAN_POINT('Ctrl Pts',(-20.4104460778757,22.8237912649708,-22.1125357446594));
#30883=CARTESIAN_POINT('Ctrl Pts',(-20.4149794470467,22.8042970353988,-22.1137715756596));
#30884=CARTESIAN_POINT('Ctrl Pts',(-20.418819011948,22.7883397702469,-22.1147780218024));
#30885=CARTESIAN_POINT('Ctrl Pts',(-20.4993754225448,22.4644456521415,-22.1351142833348));
#30886=CARTESIAN_POINT('Ctrl Pts',(-20.621051568194,22.1694235763795,-22.1520694929666));
#30887=CARTESIAN_POINT('Ctrl Pts',(-20.8714887306837,21.750397995155,-22.1797157350128));
#30888=CARTESIAN_POINT('Ctrl Pts',(-20.9705435461472,21.6110926833709,-22.1896057440371));
#30889=CARTESIAN_POINT('Ctrl Pts',(-21.0871724161455,21.4719182519041,-22.2006152295505));
#30890=CARTESIAN_POINT('Ctrl Pts',(-21.0942354072341,21.4635764873746,-22.2012796590383));
#30891=CARTESIAN_POINT('Ctrl Pts',(-21.1068688271197,21.4488087530163,-22.2024641338348));
#30892=CARTESIAN_POINT('Ctrl Pts',(-21.1124225381399,21.4423685683158,-22.2029834888604));
#30893=CARTESIAN_POINT('Ctrl Pts',(-21.1207744198263,21.4327607302075,-22.2037625418691));
#30894=CARTESIAN_POINT('Ctrl Pts',(-21.1235534683156,21.4295764411664,-22.2040214439535));
#30895=CARTESIAN_POINT('Ctrl Pts',(-21.1285153287477,21.4239135675535,-22.2044831299231));
#30896=CARTESIAN_POINT('Ctrl Pts',(-21.1306957060931,21.421432849778,-22.2046858119029));
#30897=CARTESIAN_POINT('Ctrl Pts',(-21.1350221605338,21.4165256723932,-22.2050876031595));
#30898=CARTESIAN_POINT('Ctrl Pts',(-21.1371680906735,21.4140990877062,-22.2052867061481));
#30899=CARTESIAN_POINT('Ctrl Pts',(-21.1429960429109,21.4075289176097,-22.2058269319618));
#30900=CARTESIAN_POINT('Ctrl Pts',(-21.1466850904273,21.4033916037783,-22.2061683500741));
#30901=CARTESIAN_POINT('Ctrl Pts',(-21.1604887283589,21.3879908228006,-22.2074438725158));
#30902=CARTESIAN_POINT('Ctrl Pts',(-21.1706718442596,21.3767892877239,-22.2083808715917));
#30903=CARTESIAN_POINT('Ctrl Pts',(-21.3472310480382,21.1853004347746,-22.2245607577407));
#30904=CARTESIAN_POINT('Ctrl Pts',(-21.5335417821625,21.0245582558592,-22.2407268987342));
#30905=CARTESIAN_POINT('Ctrl Pts',(-21.8697469197049,20.795599693897,-22.2681856464191));
#30906=CARTESIAN_POINT('Ctrl Pts',(-22.0099122039671,20.7148397461718,-22.2791951621481));
#30907=CARTESIAN_POINT('Ctrl Pts',(-22.2174957794679,20.6151887535421,-22.2944537454993));
#30908=CARTESIAN_POINT('Ctrl Pts',(-22.2803870449141,20.5874357950079,-22.2989465243157));
#30909=CARTESIAN_POINT('Ctrl Pts',(-22.3710855609554,20.5508312101109,-22.3051968377004));
#30910=CARTESIAN_POINT('Ctrl Pts',(-22.3981962309251,20.5403140879318,-22.3070366580032));
#30911=CARTESIAN_POINT('Ctrl Pts',(-22.4296367207027,20.5286043459448,-22.3091345933972));
#30912=CARTESIAN_POINT('Ctrl Pts',(-22.4338300394943,20.5270525095698,-22.3094136733833));
#30913=CARTESIAN_POINT('Ctrl Pts',(-22.4401916452302,20.5247132885132,-22.3098359422587));
#30914=CARTESIAN_POINT('Ctrl Pts',(-22.4423575483699,20.5239195047966,-22.309979513793));
#30915=CARTESIAN_POINT('Ctrl Pts',(-22.4461086046771,20.5225493434977,-22.3102278187852));
#30916=CARTESIAN_POINT('Ctrl Pts',(-22.4476933551452,20.5219718859087,-22.3103326173423));
#30917=CARTESIAN_POINT('Ctrl Pts',(-22.45100106165,20.5207695515296,-22.3105511331885));
#30918=CARTESIAN_POINT('Ctrl Pts',(-22.4527240926247,20.5201449020917,-22.3106648365326));
#30919=CARTESIAN_POINT('Ctrl Pts',(-22.4574901314118,20.5184216713449,-22.3109790067883));
#30920=CARTESIAN_POINT('Ctrl Pts',(-22.4605342728149,20.5173261979826,-22.311179286718));
#30921=CARTESIAN_POINT('Ctrl Pts',(-22.4724754285981,20.5130493188071,-22.3119634273581));
#30922=CARTESIAN_POINT('Ctrl Pts',(-22.4813848822013,20.5099024213506,-22.3125452429396));
#30923=CARTESIAN_POINT('Ctrl Pts',(-22.6425551330899,20.453771695304,-22.3230138975153));
#30924=CARTESIAN_POINT('Ctrl Pts',(-22.7985906006926,20.4122391139406,-22.3322481636096));
#30925=CARTESIAN_POINT('Ctrl Pts',(-23.1883914644191,20.3392487310983,-22.3545822653536));
#30926=CARTESIAN_POINT('Ctrl Pts',(-23.4237180835813,20.3214020566671,-22.3674874568137));
#30927=CARTESIAN_POINT('Ctrl Pts',(-23.7499164386583,20.3324043209362,-22.3864177524965));
#30928=CARTESIAN_POINT('Ctrl Pts',(-23.8407644591052,20.3393315878012,-22.3917944468746));
#30929=CARTESIAN_POINT('Ctrl Pts',(-23.9464573630477,20.3519130184907,-22.398221937255));
#30930=CARTESIAN_POINT('Ctrl Pts',(-23.9617097791744,20.3538394121238,-22.3991536511769));
#30931=CARTESIAN_POINT('Ctrl Pts',(-23.984586234049,20.3568951782322,-22.4005575746691));
#30932=CARTESIAN_POINT('Ctrl Pts',(-23.9922211038699,20.3579429083177,-22.4010272113882));
#30933=CARTESIAN_POINT('Ctrl Pts',(-24.0045052592011,20.3596735710986,-22.4017846116739));
#30934=CARTESIAN_POINT('Ctrl Pts',(-24.0091569687946,20.3603393100713,-22.4020718311482));
#30935=CARTESIAN_POINT('Ctrl Pts',(-24.0180446190865,20.3616311272855,-22.4026213900905));
#30936=CARTESIAN_POINT('Ctrl Pts',(-24.0222808037251,20.3622554790288,-22.4028836743489));
#30937=CARTESIAN_POINT('Ctrl Pts',(-24.0297907524361,20.3633776325662,-22.403349269258));
#30938=CARTESIAN_POINT('Ctrl Pts',(-24.0330650235965,20.3638720419574,-22.4035524719394));
#30939=CARTESIAN_POINT('Ctrl Pts',(-24.0395184437997,20.3648566729222,-22.4039533852735));
#30940=CARTESIAN_POINT('Ctrl Pts',(-24.0426976331161,20.3653466097258,-22.4041510866695));
#30941=CARTESIAN_POINT('Ctrl Pts',(-24.0503412688073,20.3665362694543,-22.4046268907203));
#30942=CARTESIAN_POINT('Ctrl Pts',(-24.0548049787478,20.3672406229375,-22.4049051403399));
#30943=CARTESIAN_POINT('Ctrl Pts',(-24.0684727828529,20.3694268141911,-22.4057583418736));
#30944=CARTESIAN_POINT('Ctrl Pts',(-24.0776718795837,20.3709391935063,-22.4063342643318));
#30945=CARTESIAN_POINT('Ctrl Pts',(-24.1831985764392,20.3887589276751,-22.4129604248652));
#30946=CARTESIAN_POINT('Ctrl Pts',(-24.2787338466558,20.409396894292,-22.4191484314502));
#30947=CARTESIAN_POINT('Ctrl Pts',(-24.6562743756093,20.5091067539253,-22.4444034379211));
#30948=CARTESIAN_POINT('Ctrl Pts',(-24.9278407102093,20.622104443896,-22.4645516423158));
#30949=CARTESIAN_POINT('Ctrl Pts',(-25.2183526124583,20.7924453775195,-22.4870477004555));
#30950=CARTESIAN_POINT('Ctrl Pts',(-25.2558947877275,20.8155052021426,-22.4899708975063));
#30951=CARTESIAN_POINT('Ctrl Pts',(-25.3504179741635,20.876268856528,-22.4973518930931));
#30952=CARTESIAN_POINT('Ctrl Pts',(-25.406698315013,20.9150305344662,-22.5017668269316));
#30953=CARTESIAN_POINT('Ctrl Pts',(-25.4705533180176,20.9620710964141,-22.5067614536495));
#30954=CARTESIAN_POINT('Ctrl Pts',(-25.4793650304505,20.9686322599755,-22.5074503534089));
#30955=CARTESIAN_POINT('Ctrl Pts',(-25.4907789477068,20.9772220862221,-22.5083420659091));
#30956=CARTESIAN_POINT('Ctrl Pts',(-25.4934116919839,20.979209762197,-22.5085477054076));
#30957=CARTESIAN_POINT('Ctrl Pts',(-25.4976757873681,20.9824393707813,-22.5088806898453));
#30958=CARTESIAN_POINT('Ctrl Pts',(-25.499309004844,20.9836788174544,-22.5090082098281));
#30959=CARTESIAN_POINT('Ctrl Pts',(-25.5024427955972,20.9860617635761,-22.5092528558147));
#30960=CARTESIAN_POINT('Ctrl Pts',(-25.503943543149,20.9872050187607,-22.509369998168));
#30961=CARTESIAN_POINT('Ctrl Pts',(-25.5073929143402,20.9898375067354,-22.509639205631));
#30962=CARTESIAN_POINT('Ctrl Pts',(-25.5093408473018,20.9913276501934,-22.5097912059474));
#30963=CARTESIAN_POINT('Ctrl Pts',(-25.5153680517507,20.9959492994993,-22.5102614417154));
#30964=CARTESIAN_POINT('Ctrl Pts',(-25.5194415558037,20.9990883665801,-22.5105791430952));
#30965=CARTESIAN_POINT('Ctrl Pts',(-25.5527520741753,21.024884972679,-22.5131763694091));
#30966=CARTESIAN_POINT('Ctrl Pts',(-25.5816060543516,21.0480357387641,-22.5154214839654));
#30967=CARTESIAN_POINT('Ctrl Pts',(-25.84900541703,21.2702564431668,-22.5362520093319));
#30968=CARTESIAN_POINT('Ctrl Pts',(-26.0580176865049,21.5023700042413,-22.5528513493944));
#30969=CARTESIAN_POINT('Ctrl Pts',(-26.2867160089689,21.8449354740634,-22.576283474658));
#30970=CARTESIAN_POINT('Ctrl Pts',(-26.338858591901,21.9316073264418,-22.5821211116812));
#30971=CARTESIAN_POINT('Ctrl Pts',(-26.4175808921299,22.0775881193931,-22.5919299012059));
#30972=CARTESIAN_POINT('Ctrl Pts',(-26.4465953681807,22.135505322366,-22.595815165304));
#30973=CARTESIAN_POINT('Ctrl Pts',(-26.477391902091,22.2019039958053,-22.6002766210332));
#30974=CARTESIAN_POINT('Ctrl Pts',(-26.4809098412002,22.2095674828963,-22.6007916448927));
#30975=CARTESIAN_POINT('Ctrl Pts',(-26.4861461764844,22.2210934217465,-22.6015664247636));
#30976=CARTESIAN_POINT('Ctrl Pts',(-26.4878871345634,22.2249456340914,-22.6018254026813));
#30977=CARTESIAN_POINT('Ctrl Pts',(-26.4908671729878,22.231574277607,-22.602271091526));
#30978=CARTESIAN_POINT('Ctrl Pts',(-26.492109916119,22.2343490641126,-22.6024576761554));
#30979=CARTESIAN_POINT('Ctrl Pts',(-26.4946601511432,22.2400648763471,-22.6028420603));
#30980=CARTESIAN_POINT('Ctrl Pts',(-26.4959671672635,22.2430061098749,-22.6030398759272));
#30981=CARTESIAN_POINT('Ctrl Pts',(-26.499101432582,22.250087847935,-22.6035162155664));
#30982=CARTESIAN_POINT('Ctrl Pts',(-26.5009243666712,22.2542302451921,-22.6037948872714));
#30983=CARTESIAN_POINT('Ctrl Pts',(-26.5064867819824,22.2669427288128,-22.6046502295817));
#30984=CARTESIAN_POINT('Ctrl Pts',(-26.510197671278,22.2755252038144,-22.6052278774032));
#30985=CARTESIAN_POINT('Ctrl Pts',(-26.5527125970797,22.3750395778857,-22.6119281692793));
#30986=CARTESIAN_POINT('Ctrl Pts',(-26.5873460708224,22.4676855344679,-22.6181919371124));
#30987=CARTESIAN_POINT('Ctrl Pts',(-26.7071661627195,22.839505168941,-22.6434698477019));
#30988=CARTESIAN_POINT('Ctrl Pts',(-26.7585223642132,23.1280919144093,-22.663549565601));
#30989=CARTESIAN_POINT('Ctrl Pts',(-26.772136978605,23.4635554195908,-22.685975446283));
#30990=CARTESIAN_POINT('Ctrl Pts',(-26.7730207433517,23.50757800266,-22.6888966099604));
#30991=CARTESIAN_POINT('Ctrl Pts',(-26.7729868457769,23.5882685850411,-22.6941963218512));
#30992=CARTESIAN_POINT('Ctrl Pts',(-26.7723458367552,23.6249294294618,-22.6965835148852));
#30993=CARTESIAN_POINT('Ctrl Pts',(-26.7697304455335,23.7006004617766,-22.7014578437141));
#30994=CARTESIAN_POINT('Ctrl Pts',(-26.7676722180439,23.7396025834573,-22.7039410043959));
#30995=CARTESIAN_POINT('Ctrl Pts',(-26.7645354487264,23.7837694899968,-22.7067126891186));
#30996=CARTESIAN_POINT('Ctrl Pts',(-26.7641527835129,23.7889783426434,-22.7070389326534));
#30997=CARTESIAN_POINT('Ctrl Pts',(-26.7635705941746,23.7966479179911,-22.7075183363536));
#30998=CARTESIAN_POINT('Ctrl Pts',(-26.7633809050503,23.7991093449085,-22.707672047434));
#30999=CARTESIAN_POINT('Ctrl Pts',(-26.763041067835,23.8034539403822,-22.7079430981767));
#31000=CARTESIAN_POINT('Ctrl Pts',(-26.7628920921192,23.8053371964363,-22.7080605043695));
#31001=CARTESIAN_POINT('Ctrl Pts',(-26.7625785682289,23.8092567226198,-22.7083046749269));
#31002=CARTESIAN_POINT('Ctrl Pts',(-26.7624137401219,23.8112929635124,-22.7084314229993));
#31003=CARTESIAN_POINT('Ctrl Pts',(-26.7619803831732,23.8165839720135,-22.7087605071955));
#31004=CARTESIAN_POINT('Ctrl Pts',(-26.7617088420718,23.8198385009681,-22.7089626725282));
#31005=CARTESIAN_POINT('Ctrl Pts',(-26.7605272084,23.8337456877951,-22.7098254876719));
#31006=CARTESIAN_POINT('Ctrl Pts',(-26.7595690423382,23.8443943538945,-22.7104834483862));
#31007=CARTESIAN_POINT('Ctrl Pts',(-26.7433140402595,24.0155014967206,-22.7210153542654));
#31008=CARTESIAN_POINT('Ctrl Pts',(-26.716050787073,24.1746205193702,-22.7302416418802));
#31009=CARTESIAN_POINT('Ctrl Pts',(-26.6368572599461,24.491753814629,-22.7486447217964));
#31010=CARTESIAN_POINT('Ctrl Pts',(-26.5843980891989,24.649122148077,-22.7577918226948));
#31011=CARTESIAN_POINT('Ctrl Pts',(-26.4524351953961,24.962269297259,-22.7770511095293));
#31012=CARTESIAN_POINT('Ctrl Pts',(-26.3719053780031,25.1170062751248,-22.7871614493294));
#31013=CARTESIAN_POINT('Ctrl Pts',(-26.2731675812366,25.274196613392,-22.7984498549883));
#31014=CARTESIAN_POINT('Ctrl Pts',(-26.2670044420189,25.2838928104908,-22.7991504352792));
#31015=CARTESIAN_POINT('Ctrl Pts',(-26.2583870673388,25.2972913482219,-22.8001245255463));
#31016=CARTESIAN_POINT('Ctrl Pts',(-26.2559767762293,25.301021963064,-22.8003963952071));
#31017=CARTESIAN_POINT('Ctrl Pts',(-26.2518188720105,25.3074284152137,-22.8008643904304));
#31018=CARTESIAN_POINT('Ctrl Pts',(-26.2500749715508,25.3101066648225,-22.8010603768324));
#31019=CARTESIAN_POINT('Ctrl Pts',(-26.2464737765852,25.3156193617767,-22.8014644802799));
#31020=CARTESIAN_POINT('Ctrl Pts',(-26.2446159904745,25.3184534812498,-22.8016726155933));
#31021=CARTESIAN_POINT('Ctrl Pts',(-26.2402921494517,25.3250270193733,-22.8021562628185));
#31022=CARTESIAN_POINT('Ctrl Pts',(-26.2378227659446,25.3287642305224,-22.8024318997627));
#31023=CARTESIAN_POINT('Ctrl Pts',(-26.2299730619153,25.3405904389913,-22.8033062796746));
#31024=CARTESIAN_POINT('Ctrl Pts',(-26.2245639906524,25.3486602050435,-22.803906107217));
#31025=CARTESIAN_POINT('Ctrl Pts',(-26.1330121703658,25.483919506964,-22.8140140667162));
#31026=CARTESIAN_POINT('Ctrl Pts',(-26.0379341571727,25.6047945216122,-22.8238689787797));
#31027=CARTESIAN_POINT('Ctrl Pts',(-25.7002619683624,25.9761374762792,-22.8569896490296));
#31028=CARTESIAN_POINT('Ctrl Pts',(-25.4257097716327,26.1941305322913,-22.8814493374239));
#31029=CARTESIAN_POINT('Ctrl Pts',(-25.1106236739297,26.3700961466631,-22.9042155777417));
#31030=CARTESIAN_POINT('Ctrl Pts',(-25.0995940299229,26.3761713289563,-22.9050060958647));
#31031=CARTESIAN_POINT('Ctrl Pts',(-25.0853438738055,26.3839118744868,-22.9060189158784));
#31032=CARTESIAN_POINT('Ctrl Pts',(-25.0821559648528,26.3856365570787,-22.9062449479937));
#31033=CARTESIAN_POINT('Ctrl Pts',(-25.0772826362361,26.3882624462306,-22.9065896397084));
#31034=CARTESIAN_POINT('Ctrl Pts',(-25.0755993268697,26.3891675303647,-22.9067085475171));
#31035=CARTESIAN_POINT('Ctrl Pts',(-25.0724374616398,26.3908639824054,-22.9069316107981));
#31036=CARTESIAN_POINT('Ctrl Pts',(-25.0709590988323,26.3916556906217,-22.9070357878665));
#31037=CARTESIAN_POINT('Ctrl Pts',(-25.0675588621271,26.3934732069059,-22.9072751231185));
#31038=CARTESIAN_POINT('Ctrl Pts',(-25.0656365691545,26.3944982185858,-22.907410229711));
#31039=CARTESIAN_POINT('Ctrl Pts',(-25.0604631273468,26.3972500854708,-22.9077733081871));
#31040=CARTESIAN_POINT('Ctrl Pts',(-25.0572100441796,26.3989733271245,-22.9080010489538));
#31041=CARTESIAN_POINT('Ctrl Pts',(-25.0400204451453,26.4080414145497,-22.9092015126386));
#31042=CARTESIAN_POINT('Ctrl Pts',(-25.0260328507375,26.415289740652,-22.9101681701937));
#31043=CARTESIAN_POINT('Ctrl Pts',(-24.8859889699608,26.4865622623997,-22.9197507232165));
#31044=CARTESIAN_POINT('Ctrl Pts',(-24.755884463948,26.5423369241634,-22.9278866877654));
#31045=CARTESIAN_POINT('Ctrl Pts',(-24.3701408559078,26.6784349823802,-22.9509977928228));
#31046=CARTESIAN_POINT('Ctrl Pts',(-24.1076669459429,26.7356929347805,-22.9655919263457));
#31047=CARTESIAN_POINT('Ctrl Pts',(-23.8180432194035,26.761941063838,-22.9825954544098));
#31048=CARTESIAN_POINT('Ctrl Pts',(-23.7949319314773,26.763784394633,-22.9839575931272));
#31049=CARTESIAN_POINT('Ctrl Pts',(-23.7668247338159,26.7657212294362,-22.9856215356915));
#31050=CARTESIAN_POINT('Ctrl Pts',(-23.761845539337,26.7660527219462,-22.9859165832064));
#31051=CARTESIAN_POINT('Ctrl Pts',(-23.7528971413496,26.766627593538,-22.9864473455226));
#31052=CARTESIAN_POINT('Ctrl Pts',(-23.7489282126842,26.76687519372,-22.9866829393556));
#31053=CARTESIAN_POINT('Ctrl Pts',(-23.7323990068503,26.7678756531333,-22.9876648783597));
#31054=CARTESIAN_POINT('Ctrl Pts',(-23.7198349504412,26.7685622878976,-22.9884131207696));
#31055=CARTESIAN_POINT('Ctrl Pts',(-23.7058963963234,26.7692421921015,-22.9892453970211));
#31056=CARTESIAN_POINT('Ctrl Pts',(-23.7045254307468,26.7693081880965,-22.9893272812253));
#31057=CARTESIAN_POINT('Ctrl Pts',(-23.6580778014003,26.7715143589604,-22.9921022723057));
#31058=CARTESIAN_POINT('Ctrl Pts',(-23.6129630348448,26.7727082921353,-22.9948231097119));
#31059=CARTESIAN_POINT('Ctrl Pts',(-23.5603646302011,26.7729953366416,-22.9980295912592));
#31060=CARTESIAN_POINT('Ctrl Pts',(-23.5528894548801,26.7730101221017,-22.9984860944758));
#31061=CARTESIAN_POINT('Ctrl Pts',(-23.5409690229497,26.7729922264102,-22.9992153727805));
#31062=CARTESIAN_POINT('Ctrl Pts',(-23.5365237372036,26.7729763553131,-22.9994876200081));
#31063=CARTESIAN_POINT('Ctrl Pts',(-23.5286829597378,26.7729321382073,-22.9999683370897));
#31064=CARTESIAN_POINT('Ctrl Pts',(-23.5252874461512,26.7729076229246,-23.000176686377));
#31065=CARTESIAN_POINT('Ctrl Pts',(-23.5182719947586,26.7728458838134,-23.0006075110921));
#31066=CARTESIAN_POINT('Ctrl Pts',(-23.5146520696526,26.7728079268422,-23.0008300092449));
#31067=CARTESIAN_POINT('Ctrl Pts',(-23.505394846672,26.7726952597143,-23.0013995068685));
#31068=CARTESIAN_POINT('Ctrl Pts',(-23.4997576840611,26.7726118563182,-23.0017467788382));
#31069=CARTESIAN_POINT('Ctrl Pts',(-23.4771811972381,26.7722185743032,-23.0031395164502));
#31070=CARTESIAN_POINT('Ctrl Pts',(-23.4602444537164,26.771789917463,-23.0041887047578));
#31071=CARTESIAN_POINT('Ctrl Pts',(-23.2428367908804,26.7645717116391,-23.0177142215618));
#31072=CARTESIAN_POINT('Ctrl Pts',(-23.0434595817204,26.739215704591,-23.0307904312862));
#31073=CARTESIAN_POINT('Ctrl Pts',(-22.6068056477271,26.6416894557977,-23.0607760366606));
#31074=CARTESIAN_POINT('Ctrl Pts',(-22.3728339085912,26.5603625911807,-23.0777932701458));
#31075=CARTESIAN_POINT('Ctrl Pts',(-22.125143031498,26.4409218748691,-23.0956529254266));
#31076=CARTESIAN_POINT('Ctrl Pts',(-22.1000060320639,26.4283928048774,-23.0974625602433));
#31077=CARTESIAN_POINT('Ctrl Pts',(-22.0750360144199,26.4155367740794,-23.0992549867839));
#31078=CARTESIAN_POINT('',(-26.7730012443091,23.5473068706377,-22.9355715880467));
#31079=CARTESIAN_POINT('Ctrl Pts',(-22.0750361484425,26.4155368430821,-23.3437344129902));
#31080=CARTESIAN_POINT('Ctrl Pts',(-22.1543302484992,26.4563620955829,-23.3377326299496));
#31081=CARTESIAN_POINT('Ctrl Pts',(-22.2353057299858,26.4938889063458,-23.3316846705842));
#31082=CARTESIAN_POINT('Ctrl Pts',(-22.3515899437915,26.5420189682118,-23.3231716910793));
#31083=CARTESIAN_POINT('Ctrl Pts',(-22.3856604926154,26.5554453451948,-23.3206978419997));
#31084=CARTESIAN_POINT('Ctrl Pts',(-22.5584381225785,26.6201531651689,-23.3082736710153));
#31085=CARTESIAN_POINT('Ctrl Pts',(-22.7003488752546,26.6624320289286,-23.2984514763994));
#31086=CARTESIAN_POINT('Ctrl Pts',(-22.8538398457921,26.6968721597427,-23.2885584840002));
#31087=CARTESIAN_POINT('Ctrl Pts',(-22.863009975991,26.6988876943567,-23.2879701886605));
#31088=CARTESIAN_POINT('Ctrl Pts',(-22.8753429596897,26.7015419568132,-23.2871827974317));
#31089=CARTESIAN_POINT('Ctrl Pts',(-22.8784980352251,26.7022160257628,-23.2869816983835));
#31090=CARTESIAN_POINT('Ctrl Pts',(-22.8834453200635,26.7032652271434,-23.2866668972446));
#31091=CARTESIAN_POINT('Ctrl Pts',(-22.8852368348243,26.7036435696253,-23.2865530101173));
#31092=CARTESIAN_POINT('Ctrl Pts',(-22.8886797905262,26.7043676084447,-23.2863343509322));
#31093=CARTESIAN_POINT('Ctrl Pts',(-22.8903311697055,26.7047135324434,-23.2862295664448));
#31094=CARTESIAN_POINT('Ctrl Pts',(-22.8942448496883,26.705530145969,-23.2859814527794));
#31095=CARTESIAN_POINT('Ctrl Pts',(-22.8965073832397,26.7059996988398,-23.285838189936));
#31096=CARTESIAN_POINT('Ctrl Pts',(-22.9011945822367,26.7069671953348,-23.2855417545288));
#31097=CARTESIAN_POINT('Ctrl Pts',(-22.9036193214394,26.7074647800062,-23.2853886026682));
#31098=CARTESIAN_POINT('Ctrl Pts',(-22.9171067210718,26.7102163618196,-23.2845377942743));
#31099=CARTESIAN_POINT('Ctrl Pts',(-22.9281807773505,26.7124150459538,-23.2838432832541));
#31100=CARTESIAN_POINT('Ctrl Pts',(-23.0275484942144,26.7316016730653,-23.2776459162308));
#31101=CARTESIAN_POINT('Ctrl Pts',(-23.1165147249962,26.7449476238273,-23.2723407839918));
#31102=CARTESIAN_POINT('Ctrl Pts',(-23.3539589562832,26.7704623974839,-23.2585493413111));
#31103=CARTESIAN_POINT('Ctrl Pts',(-23.502919957518,26.7760931610045,-23.2502687653335));
#31104=CARTESIAN_POINT('Ctrl Pts',(-23.8247403312459,26.7659533045394,-23.2322743890422));
#31105=CARTESIAN_POINT('Ctrl Pts',(-23.9970063058847,26.7465752787333,-23.2225672313433));
#31106=CARTESIAN_POINT('Ctrl Pts',(-24.1946127648312,26.7080549793497,-23.2108064143308));
#31107=CARTESIAN_POINT('Ctrl Pts',(-24.2222815075146,26.7022825754645,-23.2091456565943));
#31108=CARTESIAN_POINT('Ctrl Pts',(-24.2606535970744,26.6937489802295,-23.2068210019945));
#31109=CARTESIAN_POINT('Ctrl Pts',(-24.2714245182402,26.6912954408591,-23.2061661179996));
#31110=CARTESIAN_POINT('Ctrl Pts',(-24.3341411064715,26.676669456014,-23.2023386694301));
#31111=CARTESIAN_POINT('Ctrl Pts',(-24.3857882501499,26.6632645189796,-23.1991296349649));
#31112=CARTESIAN_POINT('Ctrl Pts',(-24.4454922574151,26.6461756606216,-23.1953451808447));
#31113=CARTESIAN_POINT('Ctrl Pts',(-24.4538979290822,26.6437326399436,-23.1948106341046));
#31114=CARTESIAN_POINT('Ctrl Pts',(-24.466410427428,26.6400406631838,-23.1940122927583));
#31115=CARTESIAN_POINT('Ctrl Pts',(-24.4705249293541,26.6388176841933,-23.1937493487763));
#31116=CARTESIAN_POINT('Ctrl Pts',(-24.4778588634135,26.6366218172976,-23.1932798998479));
#31117=CARTESIAN_POINT('Ctrl Pts',(-24.481079245029,26.6356521011775,-23.193073499146));
#31118=CARTESIAN_POINT('Ctrl Pts',(-24.4878652416896,26.6335971215827,-23.1926380150344));
#31119=CARTESIAN_POINT('Ctrl Pts',(-24.4914305016391,26.6325107107966,-23.1924088942194));
#31120=CARTESIAN_POINT('Ctrl Pts',(-24.5008419682279,26.6296249842234,-23.1918032074181));
#31121=CARTESIAN_POINT('Ctrl Pts',(-24.5066849298983,26.6278152110047,-23.1914262981945));
#31122=CARTESIAN_POINT('Ctrl Pts',(-24.5326560747106,26.6196899184631,-23.1897470502037));
#31123=CARTESIAN_POINT('Ctrl Pts',(-24.5527267470269,26.6131936029746,-23.18843876967));
#31124=CARTESIAN_POINT('Ctrl Pts',(-24.6051755161301,26.5956466713365,-23.1849916190427));
#31125=CARTESIAN_POINT('Ctrl Pts',(-24.6374432663421,26.5842769432619,-23.1828422959884));
#31126=CARTESIAN_POINT('Ctrl Pts',(-24.7822700051024,26.5306394234577,-23.173063048558));
#31127=CARTESIAN_POINT('Ctrl Pts',(-24.8925793726503,26.4826109666879,-23.1652448269617));
#31128=CARTESIAN_POINT('Ctrl Pts',(-25.0594956457667,26.3985414361393,-23.1528508555248));
#31129=CARTESIAN_POINT('Ctrl Pts',(-25.118105459658,26.3667043831666,-23.1483854720304));
#31130=CARTESIAN_POINT('Ctrl Pts',(-25.2345253596786,26.2987041348952,-23.1393054382843));
#31131=CARTESIAN_POINT('Ctrl Pts',(-25.2922616240397,26.2624776812719,-23.1346918548936));
#31132=CARTESIAN_POINT('Ctrl Pts',(-25.5132768620722,26.1138320632949,-23.1166628307839));
#31133=CARTESIAN_POINT('Ctrl Pts',(-25.6672141940529,25.9882635002258,-23.1032677765712));
#31134=CARTESIAN_POINT('Ctrl Pts',(-25.816888091021,25.8412379422775,-23.0900453799172));
#31135=CARTESIAN_POINT('Ctrl Pts',(-25.8250826529763,25.8331013745339,-23.0893208530978));
#31136=CARTESIAN_POINT('Ctrl Pts',(-25.8357071810506,25.822438019662,-23.0883809011256));
#31137=CARTESIAN_POINT('Ctrl Pts',(-25.8381768742783,25.8199512008762,-23.0881623662984));
#31138=CARTESIAN_POINT('Ctrl Pts',(-25.8419701397486,25.8161191493069,-23.0878266569877));
#31139=CARTESIAN_POINT('Ctrl Pts',(-25.843296585398,25.814776784533,-23.087709254111));
#31140=CARTESIAN_POINT('Ctrl Pts',(-25.8459315579267,25.8121054997849,-23.0874760147539));
#31141=CARTESIAN_POINT('Ctrl Pts',(-25.8472401028373,25.8107766166778,-23.08736017714));
#31142=CARTESIAN_POINT('Ctrl Pts',(-25.8501557972171,25.807810459026,-23.0871020466033));
#31143=CARTESIAN_POINT('Ctrl Pts',(-25.8517623485075,25.8061726076749,-23.0869598013957));
#31144=CARTESIAN_POINT('Ctrl Pts',(-25.8550825182506,25.8027805136235,-23.0866657966029));
#31145=CARTESIAN_POINT('Ctrl Pts',(-25.8567958869196,25.801026026932,-23.0865140567519));
#31146=CARTESIAN_POINT('Ctrl Pts',(-25.8612325391934,25.7964725160589,-23.0861210815517));
#31147=CARTESIAN_POINT('Ctrl Pts',(-25.8639527508269,25.7936704841905,-23.0858800856075));
#31148=CARTESIAN_POINT('Ctrl Pts',(-25.8986375582182,25.757812219905,-23.0828063999308));
#31149=CARTESIAN_POINT('Ctrl Pts',(-25.9298982345772,25.7240783926522,-23.0800274411334));
#31150=CARTESIAN_POINT('Ctrl Pts',(-26.0296733339258,25.6116768480862,-23.0710829798858));
#31151=CARTESIAN_POINT('Ctrl Pts',(-26.0950967377604,25.5303458303321,-23.065096452255));
#31152=CARTESIAN_POINT('Ctrl Pts',(-26.1802537802978,25.4132733357397,-23.0569082472821));
#31153=CARTESIAN_POINT('Ctrl Pts',(-26.2034254583523,25.3801231825796,-23.054634621974));
#31154=CARTESIAN_POINT('Ctrl Pts',(-26.2498064384664,25.3110351796392,-23.0499700512583));
#31155=CARTESIAN_POINT('Ctrl Pts',(-26.2729363593846,25.2750538657302,-23.0475803555466));
#31156=CARTESIAN_POINT('Ctrl Pts',(-26.435163333622,25.0112919297063,-23.0302782132406));
#31157=CARTESIAN_POINT('Ctrl Pts',(-26.5461824979433,24.7675133211699,-23.0153178038806));
#31158=CARTESIAN_POINT('Ctrl Pts',(-26.6309612708977,24.4966351834302,-22.9981181769861));
#31159=CARTESIAN_POINT('Ctrl Pts',(-26.6359096136664,24.4803744669891,-22.9970840759802));
#31160=CARTESIAN_POINT('Ctrl Pts',(-26.6423775040256,24.4585005795346,-22.9956905973267));
#31161=CARTESIAN_POINT('Ctrl Pts',(-26.6440108870025,24.452921130451,-22.9953349486562));
#31162=CARTESIAN_POINT('Ctrl Pts',(-26.6465459070653,24.4441740845337,-22.9947770511933));
#31163=CARTESIAN_POINT('Ctrl Pts',(-26.6474578064806,24.441009454038,-22.9945751379643));
#31164=CARTESIAN_POINT('Ctrl Pts',(-26.6491965033219,24.4349405792356,-22.9941877902089));
#31165=CARTESIAN_POINT('Ctrl Pts',(-26.6500240734706,24.4320365582249,-22.9940023811295));
#31166=CARTESIAN_POINT('Ctrl Pts',(-26.6519547515945,24.4252253225707,-22.993567372968));
#31167=CARTESIAN_POINT('Ctrl Pts',(-26.6530545582607,24.4213171845209,-22.9933176665351));
#31168=CARTESIAN_POINT('Ctrl Pts',(-26.6553061656553,24.4132577764344,-22.9928024917822));
#31169=CARTESIAN_POINT('Ctrl Pts',(-26.6564570326851,24.409106256119,-22.9925369935806));
#31170=CARTESIAN_POINT('Ctrl Pts',(-26.6593963035188,24.3984202431167,-22.9918532762552));
#31171=CARTESIAN_POINT('Ctrl Pts',(-26.6611724261289,24.3918824205768,-22.9914346580724));
#31172=CARTESIAN_POINT('Ctrl Pts',(-26.67547282118,24.3385795774857,-22.9880190548841));
#31173=CARTESIAN_POINT('Ctrl Pts',(-26.6869619014288,24.2915455281374,-22.9849886551368));
#31174=CARTESIAN_POINT('Ctrl Pts',(-26.7478713260265,24.0153429171023,-22.9670848689232));
#31175=CARTESIAN_POINT('Ctrl Pts',(-26.7732153269194,23.7816376651046,-22.9514286117027));
#31176=CARTESIAN_POINT('Ctrl Pts',(-26.7730011860229,23.5473074472221,-22.935571525082));
#31177=CARTESIAN_POINT('Ctrl Pts',(-26.7730011855023,23.547306877561,-22.9355714865331));
#31178=CARTESIAN_POINT('Ctrl Pts',(-26.7728003775001,23.3276090822578,-22.9207045733762));
#31179=CARTESIAN_POINT('Ctrl Pts',(-26.7501347209482,23.1084750127466,-22.9057600612752));
#31180=CARTESIAN_POINT('Ctrl Pts',(-26.7037367314502,22.8856348350834,-22.8914137520856));
#31181=CARTESIAN_POINT('Ctrl Pts',(-26.7021072044601,22.8779494709175,-22.8909200922095));
#31182=CARTESIAN_POINT('Ctrl Pts',(-26.6996019988161,22.8663434492828,-22.8901763659116));
#31183=CARTESIAN_POINT('Ctrl Pts',(-26.6987470804627,22.862418412263,-22.8899251521466));
#31184=CARTESIAN_POINT('Ctrl Pts',(-26.6973483902526,22.8560540981733,-22.889518326956));
#31185=CARTESIAN_POINT('Ctrl Pts',(-26.6968091192338,22.8536138523415,-22.8893624610396));
#31186=CARTESIAN_POINT('Ctrl Pts',(-26.6957620427135,22.8489017652036,-22.8890617239284));
#31187=CARTESIAN_POINT('Ctrl Pts',(-26.6952546133762,22.8466298431258,-22.888916831252));
#31188=CARTESIAN_POINT('Ctrl Pts',(-26.6943357363154,22.8425365919231,-22.8886559780684));
#31189=CARTESIAN_POINT('Ctrl Pts',(-26.6939251683346,22.8407150748359,-22.8885399670474));
#31190=CARTESIAN_POINT('Ctrl Pts',(-26.6930394300623,22.8368012879112,-22.8882908516684));
#31191=CARTESIAN_POINT('Ctrl Pts',(-26.6925637547108,22.8347091412707,-22.8881577772999));
#31192=CARTESIAN_POINT('Ctrl Pts',(-26.6912776931448,22.8290787151152,-22.8877998895869));
#31193=CARTESIAN_POINT('Ctrl Pts',(-26.6904634146712,22.8255413138112,-22.8875753013522));
#31194=CARTESIAN_POINT('Ctrl Pts',(-26.6866976995619,22.8093077467031,-22.886545801855));
#31195=CARTESIAN_POINT('Ctrl Pts',(-26.6836751761912,22.7966279500662,-22.8857449440323));
#31196=CARTESIAN_POINT('Ctrl Pts',(-26.6292224870703,22.5741855080108,-22.8717473548527));
#31197=CARTESIAN_POINT('Ctrl Pts',(-26.5569019811303,22.3700604504854,-22.8596943652166));
#31198=CARTESIAN_POINT('Ctrl Pts',(-26.4445321286364,22.1319815248712,-22.8449824598423));
#31199=CARTESIAN_POINT('Ctrl Pts',(-26.423442388395,22.0897296614306,-22.8423459273967));
#31200=CARTESIAN_POINT('Ctrl Pts',(-26.3794800720187,22.0062943992213,-22.8370644887152));
#31201=CARTESIAN_POINT('Ctrl Pts',(-26.3566178877872,21.9651189217063,-22.8344202774518));
#31202=CARTESIAN_POINT('Ctrl Pts',(-26.2645595977279,21.8075574713107,-22.8241134919961));
#31203=CARTESIAN_POINT('Ctrl Pts',(-26.1889650717893,21.695086933009,-22.8163419401613));
#31204=CARTESIAN_POINT('Ctrl Pts',(-26.0727388540961,21.5436985151804,-22.8050152105764));
#31205=CARTESIAN_POINT('Ctrl Pts',(-26.037820496943,21.500569309277,-22.8016813687809));
#31206=CARTESIAN_POINT('Ctrl Pts',(-25.9975543344784,21.4533800059698,-22.7979029878526));
#31207=CARTESIAN_POINT('Ctrl Pts',(-25.9932856743992,21.4484082068935,-22.7975032399048));
#31208=CARTESIAN_POINT('Ctrl Pts',(-25.9852988997786,21.4391630419603,-22.7967567728127));
#31209=CARTESIAN_POINT('Ctrl Pts',(-25.9815846186726,21.4348863859484,-22.7964102131329));
#31210=CARTESIAN_POINT('Ctrl Pts',(-25.9754741377605,21.4278880782975,-22.795841027892));
#31211=CARTESIAN_POINT('Ctrl Pts',(-25.9730845743508,21.4251606267456,-22.7956186793406));
#31212=CARTESIAN_POINT('Ctrl Pts',(-25.9684499122763,21.4198885941401,-22.7951878793955));
#31213=CARTESIAN_POINT('Ctrl Pts',(-25.9662053868691,21.4173435136352,-22.7949794521609));
#31214=CARTESIAN_POINT('Ctrl Pts',(-25.9610206458468,21.4114831897512,-22.7944984654819));
#31215=CARTESIAN_POINT('Ctrl Pts',(-25.958077608958,21.4081704615493,-22.7942257877192));
#31216=CARTESIAN_POINT('Ctrl Pts',(-25.9488972246816,21.3978797022613,-22.7933762768347));
#31217=CARTESIAN_POINT('Ctrl Pts',(-25.9426363471087,21.3909228123472,-22.7927984518255));
#31218=CARTESIAN_POINT('Ctrl Pts',(-25.8892608807416,21.3321307638952,-22.7878850634165));
#31219=CARTESIAN_POINT('Ctrl Pts',(-25.840501389739,21.2818206595933,-22.7834794504178));
#31220=CARTESIAN_POINT('Ctrl Pts',(-25.7840972156411,21.2272961752618,-22.7784668403634));
#31221=CARTESIAN_POINT('Ctrl Pts',(-25.7780270773474,21.2214741228413,-22.7779284432822));
#31222=CARTESIAN_POINT('Ctrl Pts',(-25.7340156017128,21.1795909429222,-22.774032366782));
#31223=CARTESIAN_POINT('Ctrl Pts',(-25.6952251851088,21.1444367959534,-22.7706387021536));
#31224=CARTESIAN_POINT('Ctrl Pts',(-25.5514195601596,21.0203550600468,-22.7582038865294));
#31225=CARTESIAN_POINT('Ctrl Pts',(-25.441600349126,20.9372373757034,-22.7489728037558));
#31226=CARTESIAN_POINT('Ctrl Pts',(-25.2334901504785,20.7997361332994,-22.7321092390691));
#31227=CARTESIAN_POINT('Ctrl Pts',(-25.1370165606523,20.7429744920888,-22.7245139418115));
#31228=CARTESIAN_POINT('Ctrl Pts',(-24.9522924421158,20.6468597644665,-22.7105607750245));
#31229=CARTESIAN_POINT('Ctrl Pts',(-24.8648386668492,20.6062294232143,-22.7041847647031));
#31230=CARTESIAN_POINT('Ctrl Pts',(-24.7431982323136,20.5562197779224,-22.6957412806181));
#31231=CARTESIAN_POINT('Ctrl Pts',(-24.7104904515217,20.5433937393436,-22.6935116576367));
#31232=CARTESIAN_POINT('Ctrl Pts',(-24.6742869340785,20.5298756404884,-22.6910933781915));
#31233=CARTESIAN_POINT('Ctrl Pts',(-24.6709939802508,20.5286522092759,-22.6908738679139));
#31234=CARTESIAN_POINT('Ctrl Pts',(-24.6655533209831,20.5266409585791,-22.6905119383139));
#31235=CARTESIAN_POINT('Ctrl Pts',(-24.6634067758961,20.5258500412249,-22.6903693354379));
#31236=CARTESIAN_POINT('Ctrl Pts',(-24.6592164985863,20.5243111543888,-22.6900913369758));
#31237=CARTESIAN_POINT('Ctrl Pts',(-24.6571728479127,20.5235629684313,-22.6899559284568));
#31238=CARTESIAN_POINT('Ctrl Pts',(-24.6535530171437,20.5222418953493,-22.6897163965669));
#31239=CARTESIAN_POINT('Ctrl Pts',(-24.6519771563294,20.5216681715501,-22.6896122230664));
#31240=CARTESIAN_POINT('Ctrl Pts',(-24.6486026483565,20.5204425964479,-22.6893893721141));
#31241=CARTESIAN_POINT('Ctrl Pts',(-24.6468038735213,20.5197911184315,-22.6892707174961));
#31242=CARTESIAN_POINT('Ctrl Pts',(-24.6415868967398,20.5179068934318,-22.6889269743915));
#31243=CARTESIAN_POINT('Ctrl Pts',(-24.6381671745489,20.5166783202416,-22.6887021365802));
#31244=CARTESIAN_POINT('Ctrl Pts',(-24.6228108565534,20.5111906989171,-22.6876946447829));
#31245=CARTESIAN_POINT('Ctrl Pts',(-24.6108510645216,20.5069962249757,-22.6869158045601));
#31246=CARTESIAN_POINT('Ctrl Pts',(-24.4057015973698,20.4364035832047,-22.673650446958));
#31247=CARTESIAN_POINT('Ctrl Pts',(-24.2066202783038,20.3884401898799,-22.6621900667291));
#31248=CARTESIAN_POINT('Ctrl Pts',(-23.8381705600278,20.3360057895516,-22.6413801665487));
#31249=CARTESIAN_POINT('Ctrl Pts',(-23.6704426066887,20.3253758583211,-22.6320499743358));
#31250=CARTESIAN_POINT('Ctrl Pts',(-23.4013444491763,20.3293503723596,-22.6165610348933));
#31251=CARTESIAN_POINT('Ctrl Pts',(-23.3001660085322,20.3356237695569,-22.6106228766124));
#31252=CARTESIAN_POINT('Ctrl Pts',(-23.1675068071789,20.3501499757812,-22.6026025065283));
#31253=CARTESIAN_POINT('Ctrl Pts',(-23.1356110440366,20.3541262858049,-22.6006563674381));
#31254=CARTESIAN_POINT('Ctrl Pts',(-23.0987744492221,20.3592792226422,-22.5983865996417));
#31255=CARTESIAN_POINT('Ctrl Pts',(-23.0937696251778,20.3599913396232,-22.598077742359));
#31256=CARTESIAN_POINT('Ctrl Pts',(-23.084214182764,20.3613738921973,-22.5974871434444));
#31257=CARTESIAN_POINT('Ctrl Pts',(-23.0796632799685,20.362042300871,-22.5972054666355));
#31258=CARTESIAN_POINT('Ctrl Pts',(-23.0717426467467,20.3632229632732,-22.5967145252651));
#31259=CARTESIAN_POINT('Ctrl Pts',(-23.068372260814,20.3637308254487,-22.596505400408));
#31260=CARTESIAN_POINT('Ctrl Pts',(-23.0618754911809,20.3647203257555,-22.59610186453));
#31261=CARTESIAN_POINT('Ctrl Pts',(-23.0587489968988,20.3652012222272,-22.5959074772848));
#31262=CARTESIAN_POINT('Ctrl Pts',(-23.0513581515767,20.3663491742286,-22.5954475050245));
#31263=CARTESIAN_POINT('Ctrl Pts',(-23.0470944299762,20.3670201938672,-22.595181794229));
#31264=CARTESIAN_POINT('Ctrl Pts',(-23.0344255447255,20.3690400979818,-22.5943912155654));
#31265=CARTESIAN_POINT('Ctrl Pts',(-23.0260244132669,20.3704137140007,-22.5938655618335));
#31266=CARTESIAN_POINT('Ctrl Pts',(-22.9491108026677,20.3833024617702,-22.5890401656157));
#31267=CARTESIAN_POINT('Ctrl Pts',(-22.8809866417579,20.3969961071503,-22.5846713166027));
#31268=CARTESIAN_POINT('Ctrl Pts',(-22.8035803528494,20.4151769054354,-22.5795921230051));
#31269=CARTESIAN_POINT('Ctrl Pts',(-22.793809418934,20.4175201239353,-22.5789488741472));
#31270=CARTESIAN_POINT('Ctrl Pts',(-22.6197852984883,20.4601153770153,-22.567454718774));
#31271=CARTESIAN_POINT('Ctrl Pts',(-22.4589619049632,20.5131835509343,-22.5562123522961));
#31272=CARTESIAN_POINT('Ctrl Pts',(-22.1452239829338,20.6448586181898,-22.5332574517513));
#31273=CARTESIAN_POINT('Ctrl Pts',(-21.9929111308331,20.7235743234257,-22.5215786293772));
#31274=CARTESIAN_POINT('Ctrl Pts',(-21.7925713044868,20.8482402840512,-22.5059722793803));
#31275=CARTESIAN_POINT('Ctrl Pts',(-21.7386142739113,20.8841164647915,-22.5017446788919));
#31276=CARTESIAN_POINT('Ctrl Pts',(-21.6627523749587,20.9379246053243,-22.4958045927193));
#31277=CARTESIAN_POINT('Ctrl Pts',(-21.6399475185426,20.9545543737369,-22.494019492314));
#31278=CARTESIAN_POINT('Ctrl Pts',(-21.6138227119388,20.9741359403435,-22.4919779601419));
#31279=CARTESIAN_POINT('Ctrl Pts',(-21.6102877388902,20.9767969283644,-22.4917017924691));
#31280=CARTESIAN_POINT('Ctrl Pts',(-21.6049107665644,20.9808618756914,-22.4912818471056));
#31281=CARTESIAN_POINT('Ctrl Pts',(-21.6030648001827,20.982260540927,-22.4911376987684));
#31282=CARTESIAN_POINT('Ctrl Pts',(-21.5997339809453,20.9847899166991,-22.4908776447693));
#31283=CARTESIAN_POINT('Ctrl Pts',(-21.5982486065357,20.9859199241771,-22.4907616900062));
#31284=CARTESIAN_POINT('Ctrl Pts',(-21.5952732060118,20.9881875612122,-22.4905294496601));
#31285=CARTESIAN_POINT('Ctrl Pts',(-21.5937831969001,20.9893251959678,-22.4904131653077));
#31286=CARTESIAN_POINT('Ctrl Pts',(-21.589559629184,20.9925557636601,-22.4900835894483));
#31287=CARTESIAN_POINT('Ctrl Pts',(-21.5868284199234,20.9946517857352,-22.4898705171086));
#31288=CARTESIAN_POINT('Ctrl Pts',(-21.5753565679965,21.0034849172372,-22.4889757427796));
#31289=CARTESIAN_POINT('Ctrl Pts',(-21.5666470669536,21.0102626265829,-22.4882968888774));
#31290=CARTESIAN_POINT('Ctrl Pts',(-21.420835389869,21.1249402818868,-22.476936314317));
#31291=CARTESIAN_POINT('Ctrl Pts',(-21.2926606307792,21.243771533754,-22.4670111527853));
#31292=CARTESIAN_POINT('Ctrl Pts',(-21.0634568507896,21.4937810694765,-22.4479702786533));
#31293=CARTESIAN_POINT('Ctrl Pts',(-20.9616573277731,21.623493173148,-22.4388641258175));
#31294=CARTESIAN_POINT('Ctrl Pts',(-20.8057966314606,21.8568732588851,-22.4228995872353));
#31295=CARTESIAN_POINT('Ctrl Pts',(-20.7466379731331,21.9567303338069,-22.416187551869));
#31296=CARTESIAN_POINT('Ctrl Pts',(-20.6695108405527,22.1045616334265,-22.4062603688895));
#31297=CARTESIAN_POINT('Ctrl Pts',(-20.6470961287025,22.1501177809193,-22.403203094347));
#31298=CARTESIAN_POINT('Ctrl Pts',(-20.6224427318062,22.2033635380363,-22.3996252916015));
#31299=CARTESIAN_POINT('Ctrl Pts',(-20.6191442930036,22.2105567912829,-22.3991418581384));
#31300=CARTESIAN_POINT('Ctrl Pts',(-20.6141503931983,22.221554243623,-22.3984025956947));
#31301=CARTESIAN_POINT('Ctrl Pts',(-20.6124357412117,22.2253497376357,-22.3981474285246));
#31302=CARTESIAN_POINT('Ctrl Pts',(-20.60948558749,22.2319139807837,-22.3977060664247));
#31303=CARTESIAN_POINT('Ctrl Pts',(-20.6082466237093,22.2346811758869,-22.3975199908699));
#31304=CARTESIAN_POINT('Ctrl Pts',(-20.6056901292916,22.2404127154925,-22.3971345462204));
#31305=CARTESIAN_POINT('Ctrl Pts',(-20.6043731662223,22.243377308229,-22.3969351578765));
#31306=CARTESIAN_POINT('Ctrl Pts',(-20.601192031959,22.2505675457626,-22.3964515156698));
#31307=CARTESIAN_POINT('Ctrl Pts',(-20.5993324678859,22.2547952107367,-22.3961671041153));
#31308=CARTESIAN_POINT('Ctrl Pts',(-20.5924366759677,22.2705644842909,-22.3951060723345));
#31309=CARTESIAN_POINT('Ctrl Pts',(-20.5874590713919,22.2821314651509,-22.3943274492603));
#31310=CARTESIAN_POINT('Ctrl Pts',(-20.5034946782776,22.4804413446423,-22.3809716170596));
#31311=CARTESIAN_POINT('Ctrl Pts',(-20.4422520955118,22.6741620367655,-22.367778099392));
#31312=CARTESIAN_POINT('Ctrl Pts',(-20.3624362557347,23.0450987059174,-22.3423672900487));
#31313=CARTESIAN_POINT('Ctrl Pts',(-20.3395352696603,23.2206387530685,-22.3302943600274));
#31314=CARTESIAN_POINT('Ctrl Pts',(-20.327205866074,23.4799053754935,-22.3129198699933));
#31315=CARTESIAN_POINT('Ctrl Pts',(-20.3264622318478,23.5627702893158,-22.3074387303705));
#31316=CARTESIAN_POINT('Ctrl Pts',(-20.3302413170015,23.690477912021,-22.2991867794028));
#31317=CARTESIAN_POINT('Ctrl Pts',(-20.3325087053473,23.7353486209164,-22.2963248488783));
#31318=CARTESIAN_POINT('Ctrl Pts',(-20.3360638022641,23.7850555623404,-22.2932067464514));
#31319=CARTESIAN_POINT('Ctrl Pts',(-20.3364251240258,23.7899503541195,-22.2929002614062));
#31320=CARTESIAN_POINT('Ctrl Pts',(-20.3369809966539,23.7972534262692,-22.2924438439408));
#31321=CARTESIAN_POINT('Ctrl Pts',(-20.3371670737936,23.7996623152657,-22.2922934362927));
#31322=CARTESIAN_POINT('Ctrl Pts',(-20.3374888482222,23.803767764672,-22.2920373387685));
#31323=CARTESIAN_POINT('Ctrl Pts',(-20.3376231805611,23.8054644269529,-22.2919315713571));
#31324=CARTESIAN_POINT('Ctrl Pts',(-20.3379014221426,23.8089436791239,-22.291714824714));
#31325=CARTESIAN_POINT('Ctrl Pts',(-20.3380454708194,23.8107262518686,-22.2916038537135));
#31326=CARTESIAN_POINT('Ctrl Pts',(-20.3383951746939,23.8150093554041,-22.2913374013672));
#31327=CARTESIAN_POINT('Ctrl Pts',(-20.3386022666777,23.8175097724529,-22.2911820016016));
#31328=CARTESIAN_POINT('Ctrl Pts',(-20.3393652236529,23.82659271338,-22.290618043041));
#31329=CARTESIAN_POINT('Ctrl Pts',(-20.3399384123775,23.8331738248032,-22.2902104571092));
#31330=CARTESIAN_POINT('Ctrl Pts',(-20.3498053285582,23.9425692388969,-22.283451818093));
#31331=CARTESIAN_POINT('Ctrl Pts',(-20.3640148350406,24.044892895086,-22.2773721968987));
#31332=CARTESIAN_POINT('Ctrl Pts',(-20.4146708024058,24.314025629629,-22.2616126796113));
#31333=CARTESIAN_POINT('Ctrl Pts',(-20.4594914831987,24.4789208250043,-22.2521857994242));
#31334=CARTESIAN_POINT('Ctrl Pts',(-20.5626956300021,24.766300823851,-22.2350806753798));
#31335=CARTESIAN_POINT('Ctrl Pts',(-20.6161365021468,24.8901140105494,-22.2274708141901));
#31336=CARTESIAN_POINT('Ctrl Pts',(-20.70999532912,25.0748208890429,-22.2154135129741));
#31337=CARTESIAN_POINT('Ctrl Pts',(-20.7449939674206,25.1382994065509,-22.2111345608755));
#31338=CARTESIAN_POINT('Ctrl Pts',(-20.7986062795056,25.2282273324524,-22.2048427136954));
#31339=CARTESIAN_POINT('Ctrl Pts',(-20.8155259359901,25.2556635847532,-22.2028911116017));
#31340=CARTESIAN_POINT('Ctrl Pts',(-20.8366097723268,25.2887315642404,-22.2004979539775));
#31341=CARTESIAN_POINT('Ctrl Pts',(-20.8403848566796,25.2946101655433,-22.2000709192453));
#31342=CARTESIAN_POINT('Ctrl Pts',(-20.8463251608539,25.3037946476477,-22.1994012165683));
#31343=CARTESIAN_POINT('Ctrl Pts',(-20.8484774125457,25.3071089243828,-22.199159033901));
#31344=CARTESIAN_POINT('Ctrl Pts',(-20.8522801172308,25.3129412387021,-22.1987319374245));
#31345=CARTESIAN_POINT('Ctrl Pts',(-20.8539280162127,25.3154609426574,-22.1985471195906));
#31346=CARTESIAN_POINT('Ctrl Pts',(-20.857694356812,25.3212022497634,-22.1981253098602));
#31347=CARTESIAN_POINT('Ctrl Pts',(-20.859815050979,25.3244223632524,-22.1978882334461));
#31348=CARTESIAN_POINT('Ctrl Pts',(-20.8655384417292,25.3330790384958,-22.1972495537734));
#31349=CARTESIAN_POINT('Ctrl Pts',(-20.8691518570501,25.3385084612617,-22.1968475467653));
#31350=CARTESIAN_POINT('Ctrl Pts',(-20.8858252040093,25.363397260562,-22.1949981023802));
#31351=CARTESIAN_POINT('Ctrl Pts',(-20.8990804068363,25.3827243895842,-22.1935432809991));
#31352=CARTESIAN_POINT('Ctrl Pts',(-20.9194429969747,25.4117312169147,-22.1913309451614));
#31353=CARTESIAN_POINT('Ctrl Pts',(-20.9263958305049,25.4215188699868,-22.1905793952976));
#31354=CARTESIAN_POINT('Ctrl Pts',(-20.9404291323972,25.4410418624213,-22.1890700941812));
#31355=CARTESIAN_POINT('Ctrl Pts',(-20.947509779636,25.4507768354036,-22.1883123438282));
#31356=CARTESIAN_POINT('Ctrl Pts',(-20.9556125825063,25.4617869318254,-22.1874494390629));
#31357=CARTESIAN_POINT('Ctrl Pts',(-20.9565814384575,25.4631013205166,-22.1873463292215));
#31358=CARTESIAN_POINT('Ctrl Pts',(-20.9652495563864,25.4748421423247,-22.1864244380318));
#31359=CARTESIAN_POINT('Ctrl Pts',(-20.9730105628445,25.4852226549424,-22.1856032988037));
#31360=CARTESIAN_POINT('Ctrl Pts',(-20.983234353423,25.4987265628163,-22.1845271037257));
#31361=CARTESIAN_POINT('Ctrl Pts',(-20.9856406786778,25.5018927189918,-22.1842741989603));
#31362=CARTESIAN_POINT('Ctrl Pts',(-20.9910715836346,25.5090111196676,-22.1837042951428));
#31363=CARTESIAN_POINT('Ctrl Pts',(-20.9940994654849,25.512960821925,-22.183387171381));
#31364=CARTESIAN_POINT('Ctrl Pts',(-21.00651896264,25.5290838750406,-22.1820889198472));
#31365=CARTESIAN_POINT('Ctrl Pts',(-21.0159883702982,25.5411968059797,-22.1811048636631));
#31366=CARTESIAN_POINT('Ctrl Pts',(-21.1607908389761,25.7237160637803,-22.1661441783079));
#31367=CARTESIAN_POINT('Ctrl Pts',(-21.3129373096749,25.8800303519374,-22.1515082071629));
#31368=CARTESIAN_POINT('Ctrl Pts',(-21.5769504323395,26.1013939599233,-22.1281857935563));
#31369=CARTESIAN_POINT('Ctrl Pts',(-21.6790027218157,26.1771653807462,-22.1195921001276));
#31370=CARTESIAN_POINT('Ctrl Pts',(-21.8494620353522,26.2887404901414,-22.1061535769285));
#31371=CARTESIAN_POINT('Ctrl Pts',(-21.9151458343257,26.3284593085886,-22.1011767150081));
#31372=CARTESIAN_POINT('Ctrl Pts',(-21.9890024426792,26.3695922616609,-22.0958489200036));
#31373=CARTESIAN_POINT('Ctrl Pts',(-21.9958279678048,26.3733612138983,-22.0953590145356));
#31374=CARTESIAN_POINT('Ctrl Pts',(-22.0077159609082,26.3798693997689,-22.0945101181163));
#31375=CARTESIAN_POINT('Ctrl Pts',(-22.012772178387,26.3826198907633,-22.0941504317189));
#31376=CARTESIAN_POINT('Ctrl Pts',(-22.0201083020142,26.3865851765035,-22.0936305670834));
#31377=CARTESIAN_POINT('Ctrl Pts',(-22.0223823057429,26.3878107792722,-22.0934697016536));
#31378=CARTESIAN_POINT('Ctrl Pts',(-22.0263321811675,26.3899334893096,-22.0931907702478));
#31379=CARTESIAN_POINT('Ctrl Pts',(-22.0280073750754,26.3908318491959,-22.09307262362));
#31380=CARTESIAN_POINT('Ctrl Pts',(-22.0312457122428,26.3925647919606,-22.0928445274506));
#31381=CARTESIAN_POINT('Ctrl Pts',(-22.0328087453143,26.3933995658126,-22.0927345655403));
#31382=CARTESIAN_POINT('Ctrl Pts',(-22.0365322406288,26.3953842391471,-22.0924729243622));
#31383=CARTESIAN_POINT('Ctrl Pts',(-22.038693329655,26.3965329695922,-22.0923213202111));
#31384=CARTESIAN_POINT('Ctrl Pts',(-22.0463624827773,26.4005983227503,-22.0917841960065));
#31385=CARTESIAN_POINT('Ctrl Pts',(-22.0518777428109,26.4035014520304,-22.091399532474));
#31386=CARTESIAN_POINT('Ctrl Pts',(-22.0632703262331,26.4094561510319,-22.0906081938959));
#31387=CARTESIAN_POINT('Ctrl Pts',(-22.0691485448093,26.4125055591381,-22.0902016588721));
#31388=CARTESIAN_POINT('Ctrl Pts',(-22.0750360154714,26.4155367746208,-22.0897962101869));
#31389=CARTESIAN_POINT('Origin',(-23.5502525316942,23.5502525316942,-77.3107734492734));
#31390=CARTESIAN_POINT('',(-22.0750360153462,26.4155367745563,-20.5963779455771));
#31391=CARTESIAN_POINT('',(-22.0750362008292,26.4155368700539,-20.8439479435254));
#31392=CARTESIAN_POINT('',(-22.0750360153461,26.4155367745563,-77.3107734492734));
#31393=CARTESIAN_POINT('',(-26.7730017999178,23.5524243199183,-21.439226550727));
#31394=CARTESIAN_POINT('Ctrl Pts',(-26.7730017999178,23.5524243199183,-21.439226550727));
#31395=CARTESIAN_POINT('Ctrl Pts',(-26.7730695458364,23.4518951305702,-21.4330445306115));
#31396=CARTESIAN_POINT('Ctrl Pts',(-26.7684291602479,23.3513372290751,-21.426862510496));
#31397=CARTESIAN_POINT('Ctrl Pts',(-26.7590992073237,23.2512197997044,-21.4206804903805));
#31398=CARTESIAN_POINT('Ctrl Pts',(-26.74976893384,23.1510989304877,-21.4144982578625));
#31399=CARTESIAN_POINT('Ctrl Pts',(-26.7357488122823,23.0514189895722,-21.4083160253445));
#31400=CARTESIAN_POINT('Ctrl Pts',(-26.7171093049967,22.952644181779,-21.4021337928264));
#31401=CARTESIAN_POINT('Ctrl Pts',(-26.698464366672,22.8538405937272,-21.3959497589761));
#31402=CARTESIAN_POINT('Ctrl Pts',(-26.675197445963,22.7559430835201,-21.3897657251258));
#31403=CARTESIAN_POINT('Ctrl Pts',(-26.6474299655197,22.6594048983124,-21.3835816912755));
#31404=CARTESIAN_POINT('Ctrl Pts',(-26.6196275020893,22.562745089031,-21.3773898664419));
#31405=CARTESIAN_POINT('Ctrl Pts',(-26.5873132744722,22.4674484366389,-21.3711980416083));
#31406=CARTESIAN_POINT('Ctrl Pts',(-26.550658404634,22.3739523318608,-21.3650062167746));
#31407=CARTESIAN_POINT('Ctrl Pts',(-26.5139794964912,22.2803949122324,-21.3588103313354));
#31408=CARTESIAN_POINT('Ctrl Pts',(-26.4729544512409,22.1886407824143,-21.3526144458961));
#31409=CARTESIAN_POINT('Ctrl Pts',(-26.4278014156728,22.0991047160623,-21.3464185604568));
#31410=CARTESIAN_POINT('Ctrl Pts',(-26.3825657353556,22.0094047695711,-21.3402113345309));
#31411=CARTESIAN_POINT('Ctrl Pts',(-26.3331871808525,21.9219313698342,-21.3340041086049));
#31412=CARTESIAN_POINT('Ctrl Pts',(-26.279928637451,21.8370724710583,-21.327796882679));
#31413=CARTESIAN_POINT('Ctrl Pts',(-26.2371032800918,21.7688371714596,-21.3228056333599));
#31414=CARTESIAN_POINT('Ctrl Pts',(-26.1917700887546,21.7022918649348,-21.3178143840408));
#31415=CARTESIAN_POINT('Ctrl Pts',(-26.1440843613951,21.6376224049497,-21.3128231347217));
#31416=CARTESIAN_POINT('Ctrl Pts',(-26.0851170278193,21.5576532856711,-21.3066510434094));
#31417=CARTESIAN_POINT('Ctrl Pts',(-26.0223441438312,21.4802728672081,-21.3004789520971));
#31418=CARTESIAN_POINT('Ctrl Pts',(-25.9560210816719,21.4058656154783,-21.2943068607848));
#31419=CARTESIAN_POINT('Ctrl Pts',(-25.889787880705,21.3315591782185,-21.288143132046));
#31420=CARTESIAN_POINT('Ctrl Pts',(-25.8200143487319,21.2602182223442,-21.2819794033072));
#31421=CARTESIAN_POINT('Ctrl Pts',(-25.746998079538,21.1921968579391,-21.2758156745684));
#31422=CARTESIAN_POINT('Ctrl Pts',(-25.6740591642283,21.1242475557855,-21.2696584757217));
#31423=CARTESIAN_POINT('Ctrl Pts',(-25.5978846576295,21.0596111478621,-21.263501276875));
#31424=CARTESIAN_POINT('Ctrl Pts',(-25.5188105665381,20.9986066264104,-21.2573440780283));
#31425=CARTESIAN_POINT('Ctrl Pts',(-25.4397942738123,20.9376466955646,-21.2511913797206));
#31426=CARTESIAN_POINT('Ctrl Pts',(-25.3578829532623,20.880313637768,-21.2450386814129));
#31427=CARTESIAN_POINT('Ctrl Pts',(-25.2734467122386,20.8268870808893,-21.2388859831052));
#31428=CARTESIAN_POINT('Ctrl Pts',(-25.1890424895578,20.773480783437,-21.2327356179095));
#31429=CARTESIAN_POINT('Ctrl Pts',(-25.1021156155338,20.723978275489,-21.2265852527137));
#31430=CARTESIAN_POINT('Ctrl Pts',(-25.0130655448243,20.6786161251975,-21.220434887518));
#31431=CARTESIAN_POINT('Ctrl Pts',(-24.9240254185138,20.6332590405878,-21.2142852091458));
#31432=CARTESIAN_POINT('Ctrl Pts',(-24.8328629539827,20.5920415915724,-21.2081355307736));
#31433=CARTESIAN_POINT('Ctrl Pts',(-24.7400016940692,20.5551541204349,-21.2019858524014));
#31434=CARTESIAN_POINT('Ctrl Pts',(-24.6471259612319,20.5182609001879,-21.1958352155689));
#31435=CARTESIAN_POINT('Ctrl Pts',(-24.5525513108732,20.4856991586283,-21.1896845787365));
#31436=CARTESIAN_POINT('Ctrl Pts',(-24.4567197704975,20.4576105046441,-21.1835339419041));
#31437=CARTESIAN_POINT('Ctrl Pts',(-24.3607857105047,20.4294918017007,-21.1773767251822));
#31438=CARTESIAN_POINT('Ctrl Pts',(-24.2635924931236,20.4058558644567,-21.1712195084604));
#31439=CARTESIAN_POINT('Ctrl Pts',(-24.1655956505453,20.3867939167314,-21.1650622917386));
#31440=CARTESIAN_POINT('Ctrl Pts',(-24.0675441359299,20.3677213344235,-21.1589016399308));
#31441=CARTESIAN_POINT('Ctrl Pts',(-23.9686885330799,20.3532278865423,-21.152740988123));
#31442=CARTESIAN_POINT('Ctrl Pts',(-23.8694907840872,20.3433530164756,-21.1465803363152));
#31443=CARTESIAN_POINT('Ctrl Pts',(-23.7701270419852,20.3334616222398,-21.1404093755462));
#31444=CARTESIAN_POINT('Ctrl Pts',(-23.6704204441282,20.3282042662422,-21.1342384147771));
#31445=CARTESIAN_POINT('Ctrl Pts',(-23.5708343754725,20.3275682545416,-21.1280674540081));
#31446=CARTESIAN_POINT('Ctrl Pts',(-23.4948184594487,20.3270827748688,-21.1233570437877));
#31447=CARTESIAN_POINT('Ctrl Pts',(-23.4188728013988,20.3292888687728,-21.1186466335673));
#31448=CARTESIAN_POINT('Ctrl Pts',(-23.3432007797727,20.3341606277639,-21.1139362233469));
#31449=CARTESIAN_POINT('Ctrl Pts',(-23.2440470743816,20.340544135768,-21.1077641320346));
#31450=CARTESIAN_POINT('Ctrl Pts',(-23.1450142250939,20.3515286197181,-21.1015920407222));
#31451=CARTESIAN_POINT('Ctrl Pts',(-23.046563729059,20.3671070507901,-21.0954199494099));
#31452=CARTESIAN_POINT('Ctrl Pts',(-22.9482466237134,20.3826643746282,-21.0892562206711));
#31453=CARTESIAN_POINT('Ctrl Pts',(-22.8505107286187,20.4028032067469,-21.0830924919323));
#31454=CARTESIAN_POINT('Ctrl Pts',(-22.7538148245869,20.4274645880135,-21.0769287631936));
#31455=CARTESIAN_POINT('Ctrl Pts',(-22.65722136079,20.4520998428612,-21.0707715643469));
#31456=CARTESIAN_POINT('Ctrl Pts',(-22.5616661162353,20.481248014723,-21.0646143655002));
#31457=CARTESIAN_POINT('Ctrl Pts',(-22.4675990903657,20.5147988442729,-21.0584571666535));
#31458=CARTESIAN_POINT('Ctrl Pts',(-22.3736008217876,20.548325150201,-21.0523044683458));
#31459=CARTESIAN_POINT('Ctrl Pts',(-22.2810890170904,20.5862475702482,-21.0461517700381));
#31460=CARTESIAN_POINT('Ctrl Pts',(-22.1904989906047,20.628405877608,-21.0399990717304));
#31461=CARTESIAN_POINT('Ctrl Pts',(-22.0999433159859,20.6705481984778,-21.0338487065346));
#31462=CARTESIAN_POINT('Ctrl Pts',(-22.0113083649821,20.7169230319686,-21.0276983413389));
#31463=CARTESIAN_POINT('Ctrl Pts',(-21.9250090885254,20.7673221852901,-21.0215479761431));
#31464=CARTESIAN_POINT('Ctrl Pts',(-21.8387194492812,20.8177157104375,-21.0153982977709));
#31465=CARTESIAN_POINT('Ctrl Pts',(-21.7547653411378,20.8721324428693,-21.0092486193987));
#31466=CARTESIAN_POINT('Ctrl Pts',(-21.6735358451112,20.930318936963,-21.0030989410265));
#31467=CARTESIAN_POINT('Ctrl Pts',(-21.5922936890335,20.9885144997329,-20.9969483041941));
#31468=CARTESIAN_POINT('Ctrl Pts',(-21.5137773417076,21.0504807381733,-20.9907976673616));
#31469=CARTESIAN_POINT('Ctrl Pts',(-21.438344875672,21.1159223127356,-20.9846470305292));
#31470=CARTESIAN_POINT('Ctrl Pts',(-21.3628317127436,21.1814338960356,-20.9784898138074));
#31471=CARTESIAN_POINT('Ctrl Pts',(-21.2904093478632,21.2504279544712,-20.9723325970855));
#31472=CARTESIAN_POINT('Ctrl Pts',(-21.2214007636211,21.3225705515088,-20.9661753803637));
#31473=CARTESIAN_POINT('Ctrl Pts',(-21.1523536797726,21.3947533966057,-20.9600147285559));
#31474=CARTESIAN_POINT('Ctrl Pts',(-21.0867244547687,21.4700879509065,-20.9538540767481));
#31475=CARTESIAN_POINT('Ctrl Pts',(-21.0247959722769,21.5482068956019,-20.9476934249403));
#31476=CARTESIAN_POINT('Ctrl Pts',(-20.9627638614119,21.6264565610712,-20.9415224641713));
#31477=CARTESIAN_POINT('Ctrl Pts',(-20.9044451165975,21.7074995709584,-20.9353515034022));
#31478=CARTESIAN_POINT('Ctrl Pts',(-20.8500795374211,21.7909392101115,-20.9291805426332));
#31479=CARTESIAN_POINT('Ctrl Pts',(-20.8085812700727,21.854630253332,-20.9244701324128));
#31480=CARTESIAN_POINT('Ctrl Pts',(-20.7693854461475,21.9197170969625,-20.9197597221924));
#31481=CARTESIAN_POINT('Ctrl Pts',(-20.7325802030727,21.9860146306636,-20.915049311972));
#31482=CARTESIAN_POINT('Ctrl Pts',(-20.6843539742728,22.0728848633268,-20.9088772206597));
#31483=CARTESIAN_POINT('Ctrl Pts',(-20.6400639515799,22.1621404402705,-20.9027051293474));
#31484=CARTESIAN_POINT('Ctrl Pts',(-20.5999536803001,22.2533892968223,-20.896533038035));
#31485=CARTESIAN_POINT('Ctrl Pts',(-20.5598977544723,22.3445145201947,-20.8903693092962));
#31486=CARTESIAN_POINT('Ctrl Pts',(-20.5240104972107,22.4376272610807,-20.8842055805574));
#31487=CARTESIAN_POINT('Ctrl Pts',(-20.4924902956854,22.5323096695753,-20.8780418518187));
#31488=CARTESIAN_POINT('Ctrl Pts',(-20.4610034868554,22.6268917709445,-20.871884652972));
#31489=CARTESIAN_POINT('Ctrl Pts',(-20.4338746723418,22.7230398240079,-20.8657274541253));
#31490=CARTESIAN_POINT('Ctrl Pts',(-20.4112543328994,22.8203156368443,-20.8595702552786));
#31491=CARTESIAN_POINT('Ctrl Pts',(-20.3886505275535,22.9175203469602,-20.8534175569709));
#31492=CARTESIAN_POINT('Ctrl Pts',(-20.3705487435183,23.0158507561188,-20.8472648586632));
#31493=CARTESIAN_POINT('Ctrl Pts',(-20.3570494851434,23.1148540176884,-20.8411121603555));
#31494=CARTESIAN_POINT('Ctrl Pts',(-20.3435553457064,23.2138197370804,-20.8349617951597));
#31495=CARTESIAN_POINT('Ctrl Pts',(-20.3346603226908,23.3134573719695,-20.828811429964));
#31496=CARTESIAN_POINT('Ctrl Pts',(-20.3304135585788,23.4133052801449,-20.8226610647682));
#31497=CARTESIAN_POINT('Ctrl Pts',(-20.3261672687113,23.5131420381054,-20.816511386396));
#31498=CARTESIAN_POINT('Ctrl Pts',(-20.3265682242048,23.6131885886578,-20.8103617080238));
#31499=CARTESIAN_POINT('Ctrl Pts',(-20.3316135117881,23.7129805933118,-20.8042120296516));
#31500=CARTESIAN_POINT('Ctrl Pts',(-20.3366595857064,23.8127881510832,-20.7980613928192));
#31501=CARTESIAN_POINT('Ctrl Pts',(-20.3463514075174,23.9123406502677,-20.7919107559867));
#31502=CARTESIAN_POINT('Ctrl Pts',(-20.3606340564901,24.0111771948844,-20.7857601191542));
#31503=CARTESIAN_POINT('Ctrl Pts',(-20.3749319848969,24.1101194738413,-20.7796029024324));
#31504=CARTESIAN_POINT('Ctrl Pts',(-20.3938304854383,24.2083438379856,-20.7734456857106));
#31505=CARTESIAN_POINT('Ctrl Pts',(-20.417223197488,24.305398049792,-20.7672884689888));
#31506=CARTESIAN_POINT('Ctrl Pts',(-20.4406289602359,24.4025064077458,-20.761127817181));
#31507=CARTESIAN_POINT('Ctrl Pts',(-20.468533806416,24.4984428961431,-20.7549671653732));
#31508=CARTESIAN_POINT('Ctrl Pts',(-20.5007816151657,24.5927709688199,-20.7488065135654));
#31509=CARTESIAN_POINT('Ctrl Pts',(-20.5330833859669,24.6872568859056,-20.7426355527963));
#31510=CARTESIAN_POINT('Ctrl Pts',(-20.5697424760654,24.7801286069053,-20.7364645920273));
#31511=CARTESIAN_POINT('Ctrl Pts',(-20.6105547441904,24.8709699430451,-20.7302936312583));
#31512=CARTESIAN_POINT('Ctrl Pts',(-20.6417075147376,24.9403108405491,-20.7255832210379));
#31513=CARTESIAN_POINT('Ctrl Pts',(-20.6752791638666,25.0084691430639,-20.7208728108175));
#31514=CARTESIAN_POINT('Ctrl Pts',(-20.7111615971587,25.0752706391075,-20.7161624005971));
#31515=CARTESIAN_POINT('Ctrl Pts',(-20.758172755292,25.1627902247632,-20.7099910844564));
#31516=CARTESIAN_POINT('Ctrl Pts',(-20.8093173903843,25.2482881022242,-20.7038197683157));
#31517=CARTESIAN_POINT('Ctrl Pts',(-20.8643973761013,25.3313476009354,-20.697648452175));
#31518=CARTESIAN_POINT('Ctrl Pts',(-20.9194067984958,25.4143006915906,-20.6914850421469));
#31519=CARTESIAN_POINT('Ctrl Pts',(-20.9783413163236,25.4948212516903,-20.6853216321189));
#31520=CARTESIAN_POINT('Ctrl Pts',(-21.0409566669169,25.5725165662633,-20.6791582220908));
#31521=CARTESIAN_POINT('Ctrl Pts',(-21.1035085611367,25.650133141951,-20.6730010582571));
#31522=CARTESIAN_POINT('Ctrl Pts',(-21.169733602951,25.7249298265717,-20.6668438944234));
#31523=CARTESIAN_POINT('Ctrl Pts',(-21.2393444878606,25.7965431574693,-20.6606867305896));
#31524=CARTESIAN_POINT('Ctrl Pts',(-21.3089028324128,25.8681024366191,-20.6545342140117));
#31525=CARTESIAN_POINT('Ctrl Pts',(-21.3818416363882,25.9364828294316,-20.6483816974338));
#31526=CARTESIAN_POINT('Ctrl Pts',(-21.4578342756263,26.001355019183,-20.6422291808559));
#31527=CARTESIAN_POINT('Ctrl Pts',(-21.5337933864888,26.066198586963,-20.6360793788026));
#31528=CARTESIAN_POINT('Ctrl Pts',(-21.6128033228271,26.1275367486431,-20.6299295767492));
#31529=CARTESIAN_POINT('Ctrl Pts',(-21.6945023688294,26.185078692094,-20.6237797746958));
#31530=CARTESIAN_POINT('Ctrl Pts',(-21.7762010364686,26.2426203690577,-20.6176300011234));
#31531=CARTESIAN_POINT('Ctrl Pts',(-21.8605884378157,26.2963656070947,-20.6114802275509));
#31532=CARTESIAN_POINT('Ctrl Pts',(-21.947272332421,26.3460658379144,-20.6053304539784));
#31533=CARTESIAN_POINT('Ctrl Pts',(-21.9893355772739,26.370182808982,-20.6023462845113));
#31534=CARTESIAN_POINT('Ctrl Pts',(-22.0319391436515,26.3933479752826,-20.5993621150442));
#31535=CARTESIAN_POINT('Ctrl Pts',(-22.0750360153462,26.4155367745563,-20.5963779455771));
#31536=CARTESIAN_POINT('Ctrl Pts',(-26.7730017007064,23.5525668634057,-21.4370484864937));
#31537=CARTESIAN_POINT('Ctrl Pts',(-26.7728013093608,23.8316154713373,-21.4553107584596));
#31538=CARTESIAN_POINT('Ctrl Pts',(-26.7363625104451,24.1094214252021,-21.474563588989));
#31539=CARTESIAN_POINT('Ctrl Pts',(-26.6456384354794,24.4503328290884,-21.4979959163431));
#31540=CARTESIAN_POINT('Ctrl Pts',(-26.6242256844314,24.5209477490875,-21.5028293034063));
#31541=CARTESIAN_POINT('Ctrl Pts',(-26.5906331816968,24.6194201418758,-21.5094839514482));
#31542=CARTESIAN_POINT('Ctrl Pts',(-26.5804561887718,24.6479318275351,-21.5114003538769));
#31543=CARTESIAN_POINT('Ctrl Pts',(-26.568300543437,24.6805286737495,-21.5135759137909));
#31544=CARTESIAN_POINT('Ctrl Pts',(-26.5667136595805,24.6847569270265,-21.5138578130019));
#31545=CARTESIAN_POINT('Ctrl Pts',(-26.564299493191,24.6911486009801,-21.5142834781383));
#31546=CARTESIAN_POINT('Ctrl Pts',(-26.5634787663595,24.6933144660734,-21.51442763606));
#31547=CARTESIAN_POINT('Ctrl Pts',(-26.5619925133816,24.6972239036709,-21.5146876942772));
#31548=CARTESIAN_POINT('Ctrl Pts',(-26.5613278093555,24.6989677782819,-21.5148036437055));
#31549=CARTESIAN_POINT('Ctrl Pts',(-26.5598926804892,24.7027230851596,-21.5150532152692));
#31550=CARTESIAN_POINT('Ctrl Pts',(-26.5591217559987,24.704734317147,-21.5151868063604));
#31551=CARTESIAN_POINT('Ctrl Pts',(-26.5570332287601,24.710166684739,-21.5155474468762));
#31552=CARTESIAN_POINT('Ctrl Pts',(-26.5557117987193,24.7135863605034,-21.5157742652339));
#31553=CARTESIAN_POINT('Ctrl Pts',(-26.5495401457452,24.7294770312655,-21.5168273325627));
#31554=CARTESIAN_POINT('Ctrl Pts',(-26.5446180265116,24.7419202330133,-21.5176492994726));
#31555=CARTESIAN_POINT('Ctrl Pts',(-26.5390547833571,24.7557320790169,-21.518559116728));
#31556=CARTESIAN_POINT('Ctrl Pts',(-26.5384901352657,24.7571310936038,-21.5186512436514));
#31557=CARTESIAN_POINT('Ctrl Pts',(-26.4089853603229,25.0773537965999,-21.539731726087));
#31558=CARTESIAN_POINT('Ctrl Pts',(-26.2298219384581,25.3735459443323,-21.5579188324066));
#31559=CARTESIAN_POINT('Ctrl Pts',(-25.9701584838787,25.679440968662,-21.5808049714193));
#31560=CARTESIAN_POINT('Ctrl Pts',(-25.9319958562318,25.7220459161568,-21.5840960951235));
#31561=CARTESIAN_POINT('Ctrl Pts',(-25.8466543215041,25.8123655901543,-21.5913339516413));
#31562=CARTESIAN_POINT('Ctrl Pts',(-25.7990792618654,25.8596667612672,-21.5952939458109));
#31563=CARTESIAN_POINT('Ctrl Pts',(-25.7243926206778,25.9294260277076,-21.6014263927167));
#31564=CARTESIAN_POINT('Ctrl Pts',(-25.6983302822796,25.9529829531879,-21.6035515242263));
#31565=CARTESIAN_POINT('Ctrl Pts',(-25.6664910374549,25.9808293299509,-21.6061322825843));
#31566=CARTESIAN_POINT('Ctrl Pts',(-25.6610775274115,25.9855321504714,-21.6065705517221));
#31567=CARTESIAN_POINT('Ctrl Pts',(-25.6531699033447,25.9923554794144,-21.6072099925374));
#31568=CARTESIAN_POINT('Ctrl Pts',(-25.6506881560157,25.9944903407482,-21.6074105694397));
#31569=CARTESIAN_POINT('Ctrl Pts',(-25.6457478653105,25.9987270223518,-21.6078096383237));
#31570=CARTESIAN_POINT('Ctrl Pts',(-25.6432894017999,26.0008289301896,-21.6080081263542));
#31571=CARTESIAN_POINT('Ctrl Pts',(-25.6383808988938,26.0050127688151,-21.6084042197757));
#31572=CARTESIAN_POINT('Ctrl Pts',(-25.6359308998012,26.0070947415924,-21.608601823125));
#31573=CARTESIAN_POINT('Ctrl Pts',(-25.6300343620521,26.0120903550668,-21.6090771670718));
#31574=CARTESIAN_POINT('Ctrl Pts',(-25.6265848172344,26.0150004235031,-21.609355054009));
#31575=CARTESIAN_POINT('Ctrl Pts',(-25.6160091378937,26.0238842087383,-21.6102064178512));
#31576=CARTESIAN_POINT('Ctrl Pts',(-25.6088632993215,26.0298342976844,-21.6107808595919));
#31577=CARTESIAN_POINT('Ctrl Pts',(-25.5271073468363,26.0973126011693,-21.6173440994967));
#31578=CARTESIAN_POINT('Ctrl Pts',(-25.4497970941437,26.1554775065662,-21.6234678515026));
#31579=CARTESIAN_POINT('Ctrl Pts',(-25.2874626070312,26.2665402087721,-21.636183749382));
#31580=CARTESIAN_POINT('Ctrl Pts',(-25.2023530776515,26.3191292799408,-21.6427779895879));
#31581=CARTESIAN_POINT('Ctrl Pts',(-25.0547214746422,26.4011183524669,-21.6540624923588));
#31582=CARTESIAN_POINT('Ctrl Pts',(-24.9934449517728,26.4326227116797,-21.6587034825646));
#31583=CARTESIAN_POINT('Ctrl Pts',(-24.8087654158153,26.5202065554043,-21.6725204503512));
#31584=CARTESIAN_POINT('Ctrl Pts',(-24.6827797766678,26.5704951460938,-21.6817326098741));
#31585=CARTESIAN_POINT('Ctrl Pts',(-24.4994680262209,26.6305773012484,-21.6945737084611));
#31586=CARTESIAN_POINT('Ctrl Pts',(-24.4444653866184,26.6469919197969,-21.6983562317433));
#31587=CARTESIAN_POINT('Ctrl Pts',(-24.3389018079802,26.6754481349556,-21.7054476235642));
#31588=CARTESIAN_POINT('Ctrl Pts',(-24.2884295456229,26.6877532430825,-21.7087663453197));
#31589=CARTESIAN_POINT('Ctrl Pts',(-24.2327329042231,26.6999134225422,-21.7123339035894));
#31590=CARTESIAN_POINT('Ctrl Pts',(-24.2277848360209,26.7009815209364,-21.7126500286315));
#31591=CARTESIAN_POINT('Ctrl Pts',(-24.2204611672869,26.7025443702075,-21.7131167006382));
#31592=CARTESIAN_POINT('Ctrl Pts',(-24.218087522272,26.7030480968766,-21.7132677613898));
#31593=CARTESIAN_POINT('Ctrl Pts',(-24.2140464469816,26.7039009113762,-21.7135246120452));
#31594=CARTESIAN_POINT('Ctrl Pts',(-24.2123793085098,26.7042513579658,-21.7136304806841));
#31595=CARTESIAN_POINT('Ctrl Pts',(-24.2089650543874,26.7049662366334,-21.7138471021924));
#31596=CARTESIAN_POINT('Ctrl Pts',(-24.2072179174365,26.7053305385998,-21.7139578473314));
#31597=CARTESIAN_POINT('Ctrl Pts',(-24.2030270419204,26.7062007614792,-21.7142232452066));
#31598=CARTESIAN_POINT('Ctrl Pts',(-24.2005830120232,26.7067052965456,-21.7143778177782));
#31599=CARTESIAN_POINT('Ctrl Pts',(-24.1931303144796,26.7082347761101,-21.7148485549258));
#31600=CARTESIAN_POINT('Ctrl Pts',(-24.1881197608429,26.7092506479444,-21.7151642008028));
#31601=CARTESIAN_POINT('Ctrl Pts',(-24.1336801929353,26.7201532709657,-21.7185848069968));
#31602=CARTESIAN_POINT('Ctrl Pts',(-24.0840247638312,26.7288916167078,-21.7216253681602));
#31603=CARTESIAN_POINT('Ctrl Pts',(-24.0275432143783,26.7374701661473,-21.7250151308859));
#31604=CARTESIAN_POINT('Ctrl Pts',(-24.0209017975675,26.7384576560629,-21.7254126452682));
#31605=CARTESIAN_POINT('Ctrl Pts',(-24.0093088443239,26.7401443589875,-21.7261047322912));
#31606=CARTESIAN_POINT('Ctrl Pts',(-24.0043586997956,26.7408528132454,-21.7263996800349));
#31607=CARTESIAN_POINT('Ctrl Pts',(-23.6819820339473,26.7862252363658,-21.7455720801825));
#31608=CARTESIAN_POINT('Ctrl Pts',(-23.3596417195506,26.7832991759603,-21.7626424865299));
#31609=CARTESIAN_POINT('Ctrl Pts',(-22.972282390405,26.7215609136378,-21.7852247434321));
#31610=CARTESIAN_POINT('Ctrl Pts',(-22.9019588850543,26.7079353314881,-21.7894010835479));
#31611=CARTESIAN_POINT('Ctrl Pts',(-22.794198198009,26.683304568177,-21.7959566892817));
#31612=CARTESIAN_POINT('Ctrl Pts',(-22.7564071428748,26.6739430609185,-21.7982856517863));
#31613=CARTESIAN_POINT('Ctrl Pts',(-22.7039534540641,26.6599360281156,-21.8015641700752));
#31614=CARTESIAN_POINT('Ctrl Pts',(-22.68913952431,26.655866473029,-21.8024952331016));
#31615=CARTESIAN_POINT('Ctrl Pts',(-22.6635713130845,26.6486455914143,-21.8041113769522));
#31616=CARTESIAN_POINT('Ctrl Pts',(-22.6528032405026,26.6455437782032,-21.8047948434589));
#31617=CARTESIAN_POINT('Ctrl Pts',(-22.6375054845003,26.6410506229808,-21.8057699151429));
#31618=CARTESIAN_POINT('Ctrl Pts',(-22.6329622687593,26.6397053289395,-21.806060013364));
#31619=CARTESIAN_POINT('Ctrl Pts',(-22.6254059962958,26.637449699946,-21.8065433694009));
#31620=CARTESIAN_POINT('Ctrl Pts',(-22.6223912662697,26.6365449581686,-21.8067364437013));
#31621=CARTESIAN_POINT('Ctrl Pts',(-22.616097827797,26.634646198157,-21.807139980023));
#31622=CARTESIAN_POINT('Ctrl Pts',(-22.6128193708965,26.6336513656783,-21.8073504685501));
#31623=CARTESIAN_POINT('Ctrl Pts',(-22.6056010407122,26.6314484205112,-21.8078145160028));
#31624=CARTESIAN_POINT('Ctrl Pts',(-22.6016618898375,26.63023797624,-21.808068151283));
#31625=CARTESIAN_POINT('Ctrl Pts',(-22.5879334322225,26.6259905841027,-21.8089534982555));
#31626=CARTESIAN_POINT('Ctrl Pts',(-22.5781563786545,26.6229145179191,-21.8095864954968));
#31627=CARTESIAN_POINT('Ctrl Pts',(-22.5441376770551,26.6120329035142,-21.8117977177717));
#31628=CARTESIAN_POINT('Ctrl Pts',(-22.5199745053113,26.603986847947,-21.8133838544205));
#31629=CARTESIAN_POINT('Ctrl Pts',(-22.4902007945646,26.5936789520496,-21.8153580121245));
#31630=CARTESIAN_POINT('Ctrl Pts',(-22.4844974132162,26.5916864185549,-21.8157370776543));
#31631=CARTESIAN_POINT('Ctrl Pts',(-22.4723319156831,26.5873978589314,-21.8165475693896));
#31632=CARTESIAN_POINT('Ctrl Pts',(-22.4658714666897,26.5850972225918,-21.8169791460031));
#31633=CARTESIAN_POINT('Ctrl Pts',(-22.4578242095134,26.5822025302701,-21.8175181895506));
#31634=CARTESIAN_POINT('Ctrl Pts',(-22.4562304238111,26.5816278071118,-21.8176250206067));
#31635=CARTESIAN_POINT('Ctrl Pts',(-22.4481841114409,26.5787191143273,-21.818164725485));
#31636=CARTESIAN_POINT('Ctrl Pts',(-22.441738635235,26.5763658119985,-21.8185982326311));
#31637=CARTESIAN_POINT('Ctrl Pts',(-22.4302000172079,26.5721111455872,-21.8193764130208));
#31638=CARTESIAN_POINT('Ctrl Pts',(-22.4251040634224,26.570217438998,-21.8197208348809));
#31639=CARTESIAN_POINT('Ctrl Pts',(-22.3020719814884,26.524142872546,-21.828054271201));
#31640=CARTESIAN_POINT('Ctrl Pts',(-22.186885621001,26.4731235321204,-21.8362636789268));
#31641=CARTESIAN_POINT('Ctrl Pts',(-22.0750357083693,26.4155366165066,-21.8446295278275));
#31642=CARTESIAN_POINT('Ctrl Pts',(-22.0750360154714,26.4155367746208,-22.0897962101869));
#31643=CARTESIAN_POINT('Ctrl Pts',(-22.1397156334464,26.4488376385527,-22.0853419602089));
#31644=CARTESIAN_POINT('Ctrl Pts',(-22.2055118983304,26.4799427965672,-22.0810187234138));
#31645=CARTESIAN_POINT('Ctrl Pts',(-22.4906085190755,26.6030899893747,-22.062924202422));
#31646=CARTESIAN_POINT('Ctrl Pts',(-22.718686093474,26.672940286287,-22.0499736395622));
#31647=CARTESIAN_POINT('Ctrl Pts',(-23.0882378527218,26.7427080921484,-22.0287424396187));
#31648=CARTESIAN_POINT('Ctrl Pts',(-23.2255820122374,26.7595847278466,-22.0208104453863));
#31649=CARTESIAN_POINT('Ctrl Pts',(-23.4198999471845,26.7708594310218,-22.0092544120261));
#31650=CARTESIAN_POINT('Ctrl Pts',(-23.4762967925865,26.7726476875099,-22.0058624412068));
#31651=CARTESIAN_POINT('Ctrl Pts',(-23.5409413710247,26.7729995957803,-22.0019215788501));
#31652=CARTESIAN_POINT('Ctrl Pts',(-23.5491738437247,26.7730128658238,-22.0014187347695));
#31653=CARTESIAN_POINT('Ctrl Pts',(-23.5616271716978,26.7729852225343,-22.00065657237));
#31654=CARTESIAN_POINT('Ctrl Pts',(-23.5658480877119,26.7729675605805,-22.0003979842468));
#31655=CARTESIAN_POINT('Ctrl Pts',(-23.5731084794561,26.7729229162194,-21.9999527327249));
#31656=CARTESIAN_POINT('Ctrl Pts',(-23.5761479815624,26.7728999258742,-21.9997661949026));
#31657=CARTESIAN_POINT('Ctrl Pts',(-23.5824085913836,26.7728437138005,-21.9993816898606));
#31658=CARTESIAN_POINT('Ctrl Pts',(-23.5856296902047,26.7728099626321,-21.9991837062057));
#31659=CARTESIAN_POINT('Ctrl Pts',(-23.5933857847771,26.7727170628734,-21.9987066052624));
#31660=CARTESIAN_POINT('Ctrl Pts',(-23.5979207080045,26.7726531704836,-21.9984273392636));
#31661=CARTESIAN_POINT('Ctrl Pts',(-23.6118433162056,26.7724276189102,-21.997569010909));
#31662=CARTESIAN_POINT('Ctrl Pts',(-23.6212303787722,26.7722345086209,-21.9969889620322));
#31663=CARTESIAN_POINT('Ctrl Pts',(-23.6558430966231,26.7713711228168,-21.9948451464724));
#31664=CARTESIAN_POINT('Ctrl Pts',(-23.6810609475122,26.7704456074862,-21.9932733915553));
#31665=CARTESIAN_POINT('Ctrl Pts',(-23.7122961753202,26.7689317458183,-21.9913139675977));
#31666=CARTESIAN_POINT('Ctrl Pts',(-23.7183267197134,26.7686224750654,-21.990935081125));
#31667=CARTESIAN_POINT('Ctrl Pts',(-23.7312119980531,26.76792535096,-21.9901242719562));
#31668=CARTESIAN_POINT('Ctrl Pts',(-23.7380664238393,26.7675325383225,-21.9896921967949));
#31669=CARTESIAN_POINT('Ctrl Pts',(-23.7464124576076,26.7670274823321,-21.9891651666114));
#31670=CARTESIAN_POINT('Ctrl Pts',(-23.747905350477,26.7669360975429,-21.989070858084));
#31671=CARTESIAN_POINT('Ctrl Pts',(-23.7560517179306,26.7664317395026,-21.9885560404172));
#31672=CARTESIAN_POINT('Ctrl Pts',(-23.762703924072,26.7659991645309,-21.9881349266085));
#31673=CARTESIAN_POINT('Ctrl Pts',(-23.7783873950682,26.7649304339192,-21.9871403847978));
#31674=CARTESIAN_POINT('Ctrl Pts',(-23.7874173814534,26.7642768567907,-21.9865664254657));
#31675=CARTESIAN_POINT('Ctrl Pts',(-23.8004149113002,26.7632810413189,-21.9857383466372));
#31676=CARTESIAN_POINT('Ctrl Pts',(-23.8043848200852,26.7629694815052,-21.9854851615955));
#31677=CARTESIAN_POINT('Ctrl Pts',(-23.8135702653924,26.7622314726833,-21.9848987468561));
#31678=CARTESIAN_POINT('Ctrl Pts',(-23.8187853506972,26.7617996776732,-21.9845653563707));
#31679=CARTESIAN_POINT('Ctrl Pts',(-24.1060376848745,26.7373113889743,-21.9661769941089));
#31680=CARTESIAN_POINT('Ctrl Pts',(-24.3836388485926,26.6762163351353,-21.9469212255843));
#31681=CARTESIAN_POINT('Ctrl Pts',(-24.7244993575928,26.5525194527128,-21.9224662141823));
#31682=CARTESIAN_POINT('Ctrl Pts',(-24.7983459032414,26.5225793074199,-21.9171275469122));
#31683=CARTESIAN_POINT('Ctrl Pts',(-24.939133173161,26.459325512432,-21.9069566425914));
#31684=CARTESIAN_POINT('Ctrl Pts',(-25.0061779727307,26.4263572231912,-21.9021166597251));
#31685=CARTESIAN_POINT('Ctrl Pts',(-25.0822070053008,26.3856302047552,-21.8966819337281));
#31686=CARTESIAN_POINT('Ctrl Pts',(-25.0923625801301,26.3801196074191,-21.8959571350096));
#31687=CARTESIAN_POINT('Ctrl Pts',(-25.1054272074286,26.3729392899424,-21.8950264163969));
#31688=CARTESIAN_POINT('Ctrl Pts',(-25.1083634269068,26.3713195719645,-21.8948173525166));
#31689=CARTESIAN_POINT('Ctrl Pts',(-25.1131152074289,26.3686886473414,-21.8944792044879));
#31690=CARTESIAN_POINT('Ctrl Pts',(-25.1149323180847,26.3676802676458,-21.894349938922));
#31691=CARTESIAN_POINT('Ctrl Pts',(-25.1183903218322,26.3657569204857,-21.8941040299365));
#31692=CARTESIAN_POINT('Ctrl Pts',(-25.1200313780292,26.3648422825777,-21.8939873668676));
#31693=CARTESIAN_POINT('Ctrl Pts',(-25.1237647592908,26.3627572125379,-21.8937220435087));
#31694=CARTESIAN_POINT('Ctrl Pts',(-25.1258565759431,26.3615858819037,-21.8935734422864));
#31695=CARTESIAN_POINT('Ctrl Pts',(-25.1323467664628,26.3579421251654,-21.8931125628303));
#31696=CARTESIAN_POINT('Ctrl Pts',(-25.1367406696649,26.3554616878665,-21.8928008001684));
#31697=CARTESIAN_POINT('Ctrl Pts',(-25.1699964379025,26.3365850816795,-21.8904429896448));
#31698=CARTESIAN_POINT('Ctrl Pts',(-25.198610610142,26.3197534354784,-21.8884245651528));
#31699=CARTESIAN_POINT('Ctrl Pts',(-25.3279156407261,26.2409784477269,-21.8793268610795));
#31700=CARTESIAN_POINT('Ctrl Pts',(-25.4254208741628,26.1739601388371,-21.8725306456431));
#31701=CARTESIAN_POINT('Ctrl Pts',(-25.5788822722026,26.055545708991,-21.8615676810002));
#31702=CARTESIAN_POINT('Ctrl Pts',(-25.6370910142789,26.0072706706436,-21.8573403930705));
#31703=CARTESIAN_POINT('Ctrl Pts',(-25.8170267934989,25.8470307746364,-21.8438760508893));
#31704=CARTESIAN_POINT('Ctrl Pts',(-25.9318542899437,25.7277337505138,-21.834656128004));
#31705=CARTESIAN_POINT('Ctrl Pts',(-26.0871309389041,25.5393661561986,-21.8205538165869));
#31706=CARTESIAN_POINT('Ctrl Pts',(-26.1349962876144,25.4767580108924,-21.8159349588007));
#31707=CARTESIAN_POINT('Ctrl Pts',(-26.2056867492304,25.3769117854276,-21.8086252301833));
#31708=CARTESIAN_POINT('Ctrl Pts',(-26.2301319817349,25.3408559951559,-21.8059965936573));
#31709=CARTESIAN_POINT('Ctrl Pts',(-26.2580003163491,25.2979018036724,-21.8028736255794));
#31710=CARTESIAN_POINT('Ctrl Pts',(-26.2621396604287,25.291471714498,-21.8024063535968));
#31711=CARTESIAN_POINT('Ctrl Pts',(-26.2684434936972,25.2816022855385,-21.801689466429));
#31712=CARTESIAN_POINT('Ctrl Pts',(-26.2706244487298,25.2781734525745,-21.8014404647197));
#31713=CARTESIAN_POINT('Ctrl Pts',(-26.2745880321742,25.2719159200036,-21.8009861462325));
#31714=CARTESIAN_POINT('Ctrl Pts',(-26.2763727573436,25.2690885497574,-21.8007809076939));
#31715=CARTESIAN_POINT('Ctrl Pts',(-26.279950613076,25.2634009034132,-21.8003681165152));
#31716=CARTESIAN_POINT('Ctrl Pts',(-26.2817436556665,25.2605405771842,-21.8001605609571));
#31717=CARTESIAN_POINT('Ctrl Pts',(-26.2868292968561,25.2523993819194,-21.7995699104841));
#31718=CARTESIAN_POINT('Ctrl Pts',(-26.2901110846551,25.2471118070182,-21.799186416604));
#31719=CARTESIAN_POINT('Ctrl Pts',(-26.3039464257378,25.2246757011917,-21.7975596797204));
#31720=CARTESIAN_POINT('Ctrl Pts',(-26.3143542744461,25.2074382601876,-21.7963110904648));
#31721=CARTESIAN_POINT('Ctrl Pts',(-26.5000987177289,24.8931906863811,-21.7735668922653));
#31722=CARTESIAN_POINT('Ctrl Pts',(-26.6267595323852,24.5700826973941,-21.7501112866366));
#31723=CARTESIAN_POINT('Ctrl Pts',(-26.7318793432411,24.0852950624069,-21.7167137754285));
#31724=CARTESIAN_POINT('Ctrl Pts',(-26.7534963184788,23.9353002746372,-21.706670392128));
#31725=CARTESIAN_POINT('Ctrl Pts',(-26.7649357089465,23.7782155411509,-21.6968014624371));
#31726=CARTESIAN_POINT('Ctrl Pts',(-26.7653630820495,23.7721065698632,-21.6964186896849));
#31727=CARTESIAN_POINT('Ctrl Pts',(-26.7659486745192,23.7633786974122,-21.6958733251129));
#31728=CARTESIAN_POINT('Ctrl Pts',(-26.7661211094625,23.7607608121329,-21.6957099384551));
#31729=CARTESIAN_POINT('Ctrl Pts',(-26.76641342336,23.756238748776,-21.6954280454724));
#31730=CARTESIAN_POINT('Ctrl Pts',(-26.7665348082835,23.7543346722147,-21.6953094536784));
#31731=CARTESIAN_POINT('Ctrl Pts',(-26.7667650398001,23.7506719725173,-21.6950815289967));
#31732=CARTESIAN_POINT('Ctrl Pts',(-26.7668741348517,23.7489133713154,-21.6949721820557));
#31733=CARTESIAN_POINT('Ctrl Pts',(-26.7671289776176,23.7447500841011,-21.6947135229608));
#31734=CARTESIAN_POINT('Ctrl Pts',(-26.7672734715797,23.7423453182745,-21.6945642819705));
#31735=CARTESIAN_POINT('Ctrl Pts',(-26.7676958695233,23.7351813227336,-21.6941201623205));
#31736=CARTESIAN_POINT('Ctrl Pts',(-26.7679659114317,23.7304216090741,-21.6938257250096));
#31737=CARTESIAN_POINT('Ctrl Pts',(-26.7703569245595,23.6865571180879,-21.6911179428636));
#31738=CARTESIAN_POINT('Ctrl Pts',(-26.7717756183619,23.6474151871149,-21.6887433357252));
#31739=CARTESIAN_POINT('Ctrl Pts',(-26.772530702764,23.6054677646739,-21.6862338536634));
#31740=CARTESIAN_POINT('Ctrl Pts',(-26.7725772587729,23.6026804543206,-21.6860672713219));
#31741=CARTESIAN_POINT('Ctrl Pts',(-26.772639516561,23.5986390506592,-21.685825976303));
#31742=CARTESIAN_POINT('Ctrl Pts',(-26.7726581028293,23.5973850107663,-21.6857511360902));
#31743=CARTESIAN_POINT('Ctrl Pts',(-26.7728375379543,23.5847817897861,-21.6849993153472));
#31744=CARTESIAN_POINT('Ctrl Pts',(-26.7729391632966,23.5734316948266,-21.6843249412117));
#31745=CARTESIAN_POINT('Ctrl Pts',(-26.7729908973031,23.5593366714227,-21.6834905610337));
#31746=CARTESIAN_POINT('Ctrl Pts',(-26.7729974647922,23.5565921730349,-21.6833282408137));
#31747=CARTESIAN_POINT('Ctrl Pts',(-26.7730013448547,23.5531140046475,-21.6831227089113));
#31748=CARTESIAN_POINT('Ctrl Pts',(-26.7730019127583,23.5523803478423,-21.6830793658396));
#31749=CARTESIAN_POINT('Ctrl Pts',(-26.7730329026782,23.4807438793125,-21.6788482049968));
#31750=CARTESIAN_POINT('Ctrl Pts',(-26.7707236934208,23.4098549168674,-21.6747554572151));
#31751=CARTESIAN_POINT('Ctrl Pts',(-26.7493540991225,23.0844052198086,-21.6561719539325));
#31752=CARTESIAN_POINT('Ctrl Pts',(-26.7024350143171,22.8326051831719,-21.6423002486468));
#31753=CARTESIAN_POINT('Ctrl Pts',(-26.6094442920165,22.5350402964159,-21.6243442182658));
#31754=CARTESIAN_POINT('Ctrl Pts',(-26.5911760246669,22.4815645855389,-21.6210564753802));
#31755=CARTESIAN_POINT('Ctrl Pts',(-26.5690381891529,22.421934647947,-21.6173076367352));
#31756=CARTESIAN_POINT('Ctrl Pts',(-26.5665421212536,22.4152788741713,-21.6168880284294));
#31757=CARTESIAN_POINT('Ctrl Pts',(-26.5605982761544,22.3995876860481,-21.6158959739561));
#31758=CARTESIAN_POINT('Ctrl Pts',(-26.5571318212733,22.3905594588324,-21.6153229659559));
#31759=CARTESIAN_POINT('Ctrl Pts',(-26.5521264713762,22.3776965697511,-21.6145033464791));
#31760=CARTESIAN_POINT('Ctrl Pts',(-26.5506207356753,22.3738489980616,-21.6142577664051));
#31761=CARTESIAN_POINT('Ctrl Pts',(-26.5465918677512,22.3636121756935,-21.613603264815));
#31762=CARTESIAN_POINT('Ctrl Pts',(-26.5440557083515,22.3572281020725,-21.6131939362411));
#31763=CARTESIAN_POINT('Ctrl Pts',(-26.5247671088486,22.3091232633921,-21.6101007302464));
#31764=CARTESIAN_POINT('Ctrl Pts',(-26.5071643669126,22.2677507113663,-21.6073899435756));
#31765=CARTESIAN_POINT('Ctrl Pts',(-26.4856363195235,22.2199535691617,-21.604194264443));
#31766=CARTESIAN_POINT('Ctrl Pts',(-26.482546400603,22.21315643326,-21.6037382893228));
#31767=CARTESIAN_POINT('Ctrl Pts',(-26.4775802255011,22.2023319572768,-21.6030096885569));
#31768=CARTESIAN_POINT('Ctrl Pts',(-26.475719200706,22.1982976248817,-21.6027375891909));
#31769=CARTESIAN_POINT('Ctrl Pts',(-26.4724212354756,22.1911869859597,-21.6022570352598));
#31770=CARTESIAN_POINT('Ctrl Pts',(-26.4709877617437,22.1881090712726,-21.6020487009713));
#31771=CARTESIAN_POINT('Ctrl Pts',(-26.4680153285654,22.1817530109198,-21.60161781197));
#31772=CARTESIAN_POINT('Ctrl Pts',(-26.4664757029423,22.1784751836998,-21.601395234371));
#31773=CARTESIAN_POINT('Ctrl Pts',(-26.4625228614473,22.1700964056286,-21.6008253366974));
#31774=CARTESIAN_POINT('Ctrl Pts',(-26.4601017742897,22.1649992008574,-21.6004777434042));
#31775=CARTESIAN_POINT('Ctrl Pts',(-26.4501927696255,22.1442780094415,-21.5990610247447));
#31776=CARTESIAN_POINT('Ctrl Pts',(-26.4425924121971,22.1287083932358,-21.5979879860891));
#31777=CARTESIAN_POINT('Ctrl Pts',(-26.392136931319,22.0274283675497,-21.5909510556204));
#31778=CARTESIAN_POINT('Ctrl Pts',(-26.3456066827329,21.9436124319097,-21.5848580484688));
#31779=CARTESIAN_POINT('Ctrl Pts',(-26.2198491474801,21.7391258367661,-21.5692853668725));
#31780=CARTESIAN_POINT('Ctrl Pts',(-26.1361256380688,21.6214761123938,-21.5596621955199));
#31781=CARTESIAN_POINT('Ctrl Pts',(-25.8873866165867,21.3173736338316,-21.5331496075216));
#31782=CARTESIAN_POINT('Ctrl Pts',(-25.7082033520016,21.1437586293915,-21.5160852662097));
#31783=CARTESIAN_POINT('Ctrl Pts',(-25.4992460748774,20.9835903774546,-21.4994466633055));
#31784=CARTESIAN_POINT('Ctrl Pts',(-25.4876056828333,20.9747927217979,-21.4985296337012));
#31785=CARTESIAN_POINT('Ctrl Pts',(-25.4728687957438,20.9638112299131,-21.4973814411078));
#31786=CARTESIAN_POINT('Ctrl Pts',(-25.4698279029615,20.9615535726179,-21.4971451966096));
#31787=CARTESIAN_POINT('Ctrl Pts',(-25.4650286288935,20.9580035424827,-21.4967734248046));
#31788=CARTESIAN_POINT('Ctrl Pts',(-25.4632729150456,20.9567075952368,-21.4966376470368));
#31789=CARTESIAN_POINT('Ctrl Pts',(-25.4600291577348,20.9543183625289,-21.4963872129));
#31790=CARTESIAN_POINT('Ctrl Pts',(-25.4585414997633,20.953224579132,-21.4962725217658));
#31791=CARTESIAN_POINT('Ctrl Pts',(-25.4552208547745,20.9507875069722,-21.4960168801193));
#31792=CARTESIAN_POINT('Ctrl Pts',(-25.453387390922,20.9494448812977,-21.4958759765108));
#31793=CARTESIAN_POINT('Ctrl Pts',(-25.4480740563697,20.9455626111492,-21.4954683498485));
#31794=CARTESIAN_POINT('Ctrl Pts',(-25.4445904943156,20.9430279910007,-21.4952019778541));
#31795=CARTESIAN_POINT('Ctrl Pts',(-25.4206895748936,20.9257110069899,-21.4933803173217));
#31796=CARTESIAN_POINT('Ctrl Pts',(-25.4001037410081,20.9111611074345,-21.4918409271065));
#31797=CARTESIAN_POINT('Ctrl Pts',(-25.3361825670815,20.8670976354963,-21.4871442760681));
#31798=CARTESIAN_POINT('Ctrl Pts',(-25.2922942069247,20.8383974904788,-21.4840355794075));
#31799=CARTESIAN_POINT('Ctrl Pts',(-25.1839071833568,20.7712372361683,-21.4765859468629));
#31800=CARTESIAN_POINT('Ctrl Pts',(-25.1187260889777,20.7339348194565,-21.4722946342769));
#31801=CARTESIAN_POINT('Ctrl Pts',(-24.7466470279695,20.5379268271521,-21.4485100834268));
#31802=CARTESIAN_POINT('Ctrl Pts',(-24.4171318937395,20.4271159394865,-21.4297945584365));
#31803=CARTESIAN_POINT('Ctrl Pts',(-24.0558283625011,20.3673385663929,-21.4076524514498));
#31804=CARTESIAN_POINT('Ctrl Pts',(-24.0353222782952,20.3641490272819,-21.4063915839923));
#31805=CARTESIAN_POINT('Ctrl Pts',(-24.0085556127557,20.360250101471,-21.4047398898518));
#31806=CARTESIAN_POINT('Ctrl Pts',(-24.0023214282005,20.3593606609373,-21.4043547818353));
#31807=CARTESIAN_POINT('Ctrl Pts',(-23.9927265124743,20.3580204229073,-21.4037614190082));
#31808=CARTESIAN_POINT('Ctrl Pts',(-23.9893675854421,20.3575566442865,-21.4035535758202));
#31809=CARTESIAN_POINT('Ctrl Pts',(-23.9827278004184,20.356650542694,-21.4031424756143));
#31810=CARTESIAN_POINT('Ctrl Pts',(-23.9794469799743,20.3562079722619,-21.4029392267076));
#31811=CARTESIAN_POINT('Ctrl Pts',(-23.9722550809867,20.3552490928797,-21.4024934230672));
#31812=CARTESIAN_POINT('Ctrl Pts',(-23.9683437287578,20.3547349090917,-21.402250801366));
#31813=CARTESIAN_POINT('Ctrl Pts',(-23.9572867543433,20.3533020146955,-21.4015644528629));
#31814=CARTESIAN_POINT('Ctrl Pts',(-23.9501390148824,20.3524000857926,-21.4011201956895));
#31815=CARTESIAN_POINT('Ctrl Pts',(-23.9341432761456,20.3504361504537,-21.400124706239));
#31816=CARTESIAN_POINT('Ctrl Pts',(-23.9252938009096,20.3493868642302,-21.3995730746057));
#31817=CARTESIAN_POINT('Ctrl Pts',(-23.7470544409016,20.3290022513304,-21.3884443025886));
#31818=CARTESIAN_POINT('Ctrl Pts',(-23.5764277764343,20.3231048475553,-21.3774371080272));
#31819=CARTESIAN_POINT('Ctrl Pts',(-23.0841170963695,20.3451388637449,-21.3446999144034));
#31820=CARTESIAN_POINT('Ctrl Pts',(-22.7660831410456,20.4077843219346,-21.3221820358439));
#31821=CARTESIAN_POINT('Ctrl Pts',(-22.4476150512043,20.5219587854325,-21.3007758002489));
#31822=CARTESIAN_POINT('Ctrl Pts',(-22.4326270276535,20.527458181289,-21.2997716705232));
#31823=CARTESIAN_POINT('Ctrl Pts',(-22.4143411164558,20.5343222375458,-21.2985511974473));
#31824=CARTESIAN_POINT('Ctrl Pts',(-22.4110041710114,20.5355811639633,-21.2983286648767));
#31825=CARTESIAN_POINT('Ctrl Pts',(-22.4055008248396,20.537667848985,-21.2979619794036));
#31826=CARTESIAN_POINT('Ctrl Pts',(-22.4033332275068,20.5384924066853,-21.2978176351443));
#31827=CARTESIAN_POINT('Ctrl Pts',(-22.3994226280074,20.5399848393864,-21.2975573713165));
#31828=CARTESIAN_POINT('Ctrl Pts',(-22.3976793204664,20.5406518871917,-21.2974414022713));
#31829=CARTESIAN_POINT('Ctrl Pts',(-22.3939274272259,20.5420912251724,-21.2971919339717));
#31830=CARTESIAN_POINT('Ctrl Pts',(-22.3919190408195,20.5428640105248,-21.2970584655028));
#31831=CARTESIAN_POINT('Ctrl Pts',(-22.3864098358734,20.5449901755619,-21.2966925412369));
#31832=CARTESIAN_POINT('Ctrl Pts',(-22.3829105911449,20.5463476656946,-21.2964603337267));
#31833=CARTESIAN_POINT('Ctrl Pts',(-22.3645969279809,20.5534890656138,-21.2952461338671));
#31834=CARTESIAN_POINT('Ctrl Pts',(-22.3498227623998,20.5593765938139,-21.2942703166142));
#31835=CARTESIAN_POINT('Ctrl Pts',(-22.1660553897168,20.634189264258,-21.2821719162451));
#31836=CARTESIAN_POINT('Ctrl Pts',(-22.003142134991,20.7172512150757,-21.2718524170749));
#31837=CARTESIAN_POINT('Ctrl Pts',(-21.6671876415675,20.9262126422353,-21.2496886238375));
#31838=CARTESIAN_POINT('Ctrl Pts',(-21.4978748770997,21.0564083949596,-21.2379087859107));
#31839=CARTESIAN_POINT('Ctrl Pts',(-21.2689602879166,21.2716445074885,-21.219636835821));
#31840=CARTESIAN_POINT('Ctrl Pts',(-21.1985784868721,21.3443570705315,-21.2136355467367));
#31841=CARTESIAN_POINT('Ctrl Pts',(-21.1255210877273,21.4273103691255,-21.2069076620542));
#31842=CARTESIAN_POINT('Ctrl Pts',(-21.1193365973462,21.4343948526048,-21.2063340007468));
#31843=CARTESIAN_POINT('Ctrl Pts',(-21.1102131906344,21.4449387356408,-21.2054815345016));
#31844=CARTESIAN_POINT('Ctrl Pts',(-21.1072503937657,21.4483774831945,-21.20520372024));
#31845=CARTESIAN_POINT('Ctrl Pts',(-21.1021967574798,21.454268068025,-21.2047281702889));
#31846=CARTESIAN_POINT('Ctrl Pts',(-21.100102306204,21.4567168099964,-21.2045305840908));
#31847=CARTESIAN_POINT('Ctrl Pts',(-21.0959095523669,21.4616337064876,-21.2041340474302));
#31848=CARTESIAN_POINT('Ctrl Pts',(-21.0938112922177,21.4641018913856,-21.2039350956008));
#31849=CARTESIAN_POINT('Ctrl Pts',(-21.0889781384199,21.4698045354876,-21.203475657223));
#31850=CARTESIAN_POINT('Ctrl Pts',(-21.0862458973494,21.4730412257507,-21.203215062175));
#31851=CARTESIAN_POINT('Ctrl Pts',(-21.0780201496004,21.482824745494,-21.202427873656));
#31852=CARTESIAN_POINT('Ctrl Pts',(-21.0725463291268,21.4893880107398,-21.2019004760195));
#31853=CARTESIAN_POINT('Ctrl Pts',(-21.0600878649234,21.5044474421297,-21.2006918863166));
#31854=CARTESIAN_POINT('Ctrl Pts',(-21.0531205079773,21.5129577117385,-21.2000099986102));
#31855=CARTESIAN_POINT('Ctrl Pts',(-20.9902975642925,21.5904991592799,-21.193806614963));
#31856=CARTESIAN_POINT('Ctrl Pts',(-20.9372786560383,21.6617696125376,-21.1881722908001));
#31857=CARTESIAN_POINT('Ctrl Pts',(-20.7760781876752,21.8982682963463,-21.1696653488789));
#31858=CARTESIAN_POINT('Ctrl Pts',(-20.680122166148,22.0712569168643,-21.1563798293143));
#31859=CARTESIAN_POINT('Ctrl Pts',(-20.5175538124135,22.4405890482319,-21.1290643912704));
#31860=CARTESIAN_POINT('Ctrl Pts',(-20.4527884274916,22.6368243443284,-21.1150951347814));
#31861=CARTESIAN_POINT('Ctrl Pts',(-20.4044811009938,22.8499723424508,-21.1013110674143));
#31862=CARTESIAN_POINT('Ctrl Pts',(-20.4018192638445,22.8620387514423,-21.1005354432051));
#31863=CARTESIAN_POINT('Ctrl Pts',(-20.3984719099176,22.8776386582551,-21.0995390114092));
#31864=CARTESIAN_POINT('Ctrl Pts',(-20.3977228676956,22.8811581971943,-21.0993146184708));
#31865=CARTESIAN_POINT('Ctrl Pts',(-20.3965860826335,22.8865439183527,-21.0989718867595));
#31866=CARTESIAN_POINT('Ctrl Pts',(-20.3961941011873,22.8884091874301,-21.0988533041756));
#31867=CARTESIAN_POINT('Ctrl Pts',(-20.3954602837374,22.8919165627003,-21.0986305491103));
#31868=CARTESIAN_POINT('Ctrl Pts',(-20.3951180763147,22.893558581402,-21.0985263556083));
#31869=CARTESIAN_POINT('Ctrl Pts',(-20.3943329088923,22.8973408426373,-21.0982865654807));
#31870=CARTESIAN_POINT('Ctrl Pts',(-20.3938908448596,22.8994812652391,-21.0981510212401));
#31871=CARTESIAN_POINT('Ctrl Pts',(-20.3926648466504,22.9054480425408,-21.0977735989148));
#31872=CARTESIAN_POINT('Ctrl Pts',(-20.3918856872463,22.9092753915027,-21.0975319958077));
#31873=CARTESIAN_POINT('Ctrl Pts',(-20.3875530226601,22.9307578133918,-21.096178619143));
#31874=CARTESIAN_POINT('Ctrl Pts',(-20.3841405037507,22.9484414713543,-21.0950748291119));
#31875=CARTESIAN_POINT('Ctrl Pts',(-20.3746855123621,22.9997451241154,-21.0918997804587));
#31876=CARTESIAN_POINT('Ctrl Pts',(-20.3690288826947,23.0334347663059,-21.0898486062595));
#31877=CARTESIAN_POINT('Ctrl Pts',(-20.3492545644892,23.1638740135483,-21.0820149485816));
#31878=CARTESIAN_POINT('Ctrl Pts',(-20.3390055780899,23.2611635362846,-21.0763999868643));
#31879=CARTESIAN_POINT('Ctrl Pts',(-20.3155180158724,23.6557846864663,-21.0540189978929));
#31880=CARTESIAN_POINT('Ctrl Pts',(-20.3390530645731,23.9537905574934,-21.0378676350291));
#31881=CARTESIAN_POINT('Ctrl Pts',(-20.4042516068,24.2494110775156,-21.0199914156989));
#31882=CARTESIAN_POINT('Ctrl Pts',(-20.4053814778823,24.2544758954725,-21.0196846287967));
#31883=CARTESIAN_POINT('Ctrl Pts',(-20.4073988750514,24.2634175003758,-21.0191420896494));
#31884=CARTESIAN_POINT('Ctrl Pts',(-20.4082813555709,24.2672954229075,-21.0189064851552));
#31885=CARTESIAN_POINT('Ctrl Pts',(-20.4121824727497,24.2842927893224,-21.0178724363121));
#31886=CARTESIAN_POINT('Ctrl Pts',(-20.4152760885205,24.2973947454349,-21.0170717907858));
#31887=CARTESIAN_POINT('Ctrl Pts',(-20.4191657661327,24.3134185640695,-21.0160880485105));
#31888=CARTESIAN_POINT('Ctrl Pts',(-20.4198840045022,24.3163593194986,-21.0159073203032));
#31889=CARTESIAN_POINT('Ctrl Pts',(-20.4209229549919,24.3205873438322,-21.0156472088915));
#31890=CARTESIAN_POINT('Ctrl Pts',(-20.4212403216225,24.3218754393567,-21.0155679278589));
#31891=CARTESIAN_POINT('Ctrl Pts',(-20.4232047894374,24.3298274808054,-21.0150782620721));
#31892=CARTESIAN_POINT('Ctrl Pts',(-20.4248723740313,24.3364863090442,-21.0146672516103));
#31893=CARTESIAN_POINT('Ctrl Pts',(-20.4280450168518,24.3489853845465,-21.0138938901853));
#31894=CARTESIAN_POINT('Ctrl Pts',(-20.4295452216216,24.3548268415526,-21.0135316911908));
#31895=CARTESIAN_POINT('Ctrl Pts',(-20.4374047932153,24.3850775266208,-21.0116519667107));
#31896=CARTESIAN_POINT('Ctrl Pts',(-20.4440340388428,24.409415167225,-21.0101260336545));
#31897=CARTESIAN_POINT('Ctrl Pts',(-20.4535238946154,24.4427084710636,-21.0080189143858));
#31898=CARTESIAN_POINT('Ctrl Pts',(-20.456139128987,24.4517335928759,-21.0074457229372));
#31899=CARTESIAN_POINT('Ctrl Pts',(-20.4600756245269,24.4650994210565,-21.006593843931));
#31900=CARTESIAN_POINT('Ctrl Pts',(-20.4613666597229,24.4694490385191,-21.0063161451754));
#31901=CARTESIAN_POINT('Ctrl Pts',(-20.4635901331589,24.4768825440327,-21.0058407421613));
#31902=CARTESIAN_POINT('Ctrl Pts',(-20.4645180211027,24.4799677958101,-21.0056431871914));
#31903=CARTESIAN_POINT('Ctrl Pts',(-20.4663880891635,24.4861521817373,-21.0052467035905));
#31904=CARTESIAN_POINT('Ctrl Pts',(-20.4673303182028,24.4892512964952,-21.0050477735782));
#31905=CARTESIAN_POINT('Ctrl Pts',(-20.4695156644645,24.4964004405901,-21.0045883081232));
#31906=CARTESIAN_POINT('Ctrl Pts',(-20.4707620965587,24.5004494429982,-21.0043276640495));
#31907=CARTESIAN_POINT('Ctrl Pts',(-20.4745523240955,24.5126761082325,-21.0035393261919));
#31908=CARTESIAN_POINT('Ctrl Pts',(-20.4771207211096,24.5208460512488,-21.0030108238813));
#31909=CARTESIAN_POINT('Ctrl Pts',(-20.4830681708321,24.5395043102009,-21.0017998469576));
#31910=CARTESIAN_POINT('Ctrl Pts',(-20.4864684981775,24.5499856840432,-21.0011166745857));
#31911=CARTESIAN_POINT('Ctrl Pts',(-20.4977313881168,24.5841059280638,-20.9988831484188));
#31912=CARTESIAN_POINT('Ctrl Pts',(-20.5058141528056,24.6076706505411,-20.9973255403671));
#31913=CARTESIAN_POINT('Ctrl Pts',(-20.5390631198272,24.7010631214974,-20.9910910659739));
#31914=CARTESIAN_POINT('Ctrl Pts',(-20.5663635329161,24.7701015764511,-20.9863443010329));
#31915=CARTESIAN_POINT('Ctrl Pts',(-20.6555433113177,24.974668654292,-20.971854661949));
#31916=CARTESIAN_POINT('Ctrl Pts',(-20.7244534683802,25.1069008604537,-20.9619018762077));
#31917=CARTESIAN_POINT('Ctrl Pts',(-20.9290432972204,25.4408300253337,-20.9354521088407));
#31918=CARTESIAN_POINT('Ctrl Pts',(-21.078816841397,25.6328106460435,-20.9188262471932));
#31919=CARTESIAN_POINT('Ctrl Pts',(-21.2582956321969,25.8159174632993,-20.9026360720793));
#31920=CARTESIAN_POINT('Ctrl Pts',(-21.2679159074272,25.8256082315375,-20.9017783079509));
#31921=CARTESIAN_POINT('Ctrl Pts',(-21.2802170567106,25.837843000542,-20.9006945492155));
#31922=CARTESIAN_POINT('Ctrl Pts',(-21.2828409199592,25.8404437451397,-20.9004641273487));
#31923=CARTESIAN_POINT('Ctrl Pts',(-21.2870063867937,25.8445583348108,-20.9000995148651));
#31924=CARTESIAN_POINT('Ctrl Pts',(-21.2885450403901,25.8460751412323,-20.8999650894175));
#31925=CARTESIAN_POINT('Ctrl Pts',(-21.2912822052316,25.848768019178,-20.8997264122682));
#31926=CARTESIAN_POINT('Ctrl Pts',(-21.2924801034659,25.8499446946585,-20.8996221124508));
#31927=CARTESIAN_POINT('Ctrl Pts',(-21.2952666130387,25.8526775607714,-20.8993798541809));
#31928=CARTESIAN_POINT('Ctrl Pts',(-21.2968559132407,25.8542330411322,-20.8992419524046));
#31929=CARTESIAN_POINT('Ctrl Pts',(-21.3013664093794,25.8586384237436,-20.8988513462173));
#31930=CARTESIAN_POINT('Ctrl Pts',(-21.3042914238071,25.8614844369879,-20.8985989489147));
#31931=CARTESIAN_POINT('Ctrl Pts',(-21.3221638287181,25.8788081615754,-20.8970622152849));
#31932=CARTESIAN_POINT('Ctrl Pts',(-21.3372461958914,25.8931468104773,-20.8957886231893));
#31933=CARTESIAN_POINT('Ctrl Pts',(-21.3829141056527,25.9357283140973,-20.8919975213357));
#31934=CARTESIAN_POINT('Ctrl Pts',(-21.4139101656069,25.9635267010424,-20.8895105640596));
#31935=CARTESIAN_POINT('Ctrl Pts',(-21.4853444244239,26.0251362101969,-20.8839474901083));
#31936=CARTESIAN_POINT('Ctrl Pts',(-21.5260912709333,26.0585719751414,-20.8808913037503));
#31937=CARTESIAN_POINT('Ctrl Pts',(-21.6732027120815,26.1733670650776,-20.8701909697272));
#31938=CARTESIAN_POINT('Ctrl Pts',(-21.7837996861613,26.2490844284423,-20.8627387053836));
#31939=CARTESIAN_POINT('Ctrl Pts',(-21.9565296392942,26.3521600693959,-20.8514971429009));
#31940=CARTESIAN_POINT('Ctrl Pts',(-22.0153075857551,26.3847850779201,-20.8477367945974));
#31941=CARTESIAN_POINT('Ctrl Pts',(-22.0750362008293,26.4155368700539,-20.8439479435254));
#31942=CARTESIAN_POINT('Origin',(-23.5502525316942,23.5502525316942,-77.3107734492734));
#31943=CARTESIAN_POINT('',(-22.0750360113656,26.4155367725069,-19.3485684984428));
#31944=CARTESIAN_POINT('',(-22.075036015346,26.4155367745563,-19.592915740792));
#31945=CARTESIAN_POINT('',(-22.0750360153461,26.4155367745563,-77.3107734492734));
#31946=CARTESIAN_POINT('',(-26.7730016852365,23.5479167572311,-20.189226550727));
#31947=CARTESIAN_POINT('Ctrl Pts',(-22.0750360113656,26.4155367725069,-19.3485684984428));
#31948=CARTESIAN_POINT('Ctrl Pts',(-22.0324063855993,26.3935885387889,-19.3513199436375));
#31949=CARTESIAN_POINT('Ctrl Pts',(-21.9902669454401,26.370689129756,-19.3540423519884));
#31950=CARTESIAN_POINT('Ctrl Pts',(-21.6552252746965,26.1788121170182,-19.3758272973173));
#31951=CARTESIAN_POINT('Ctrl Pts',(-21.3901068379,25.9656645484058,-19.3942131632512));
#31952=CARTESIAN_POINT('Ctrl Pts',(-21.1496257678348,25.7004857929686,-19.4158687651846));
#31953=CARTESIAN_POINT('Ctrl Pts',(-21.1364216884345,25.6856523935268,-19.4170757169032));
#31954=CARTESIAN_POINT('Ctrl Pts',(-21.1192835353348,25.6660373995469,-19.418666396409));
#31955=CARTESIAN_POINT('Ctrl Pts',(-21.1152247582842,25.6613649422902,-19.4190449172998));
#31956=CARTESIAN_POINT('Ctrl Pts',(-21.108977545863,25.6541311772974,-19.4196303405881));
#31957=CARTESIAN_POINT('Ctrl Pts',(-21.1067796094569,25.6515780633588,-19.4198368489277));
#31958=CARTESIAN_POINT('Ctrl Pts',(-21.1024080175492,25.6464839069891,-19.4202486662474));
#31959=CARTESIAN_POINT('Ctrl Pts',(-21.1002343055045,25.643942918405,-19.4204539725238));
#31960=CARTESIAN_POINT('Ctrl Pts',(-21.0954741468798,25.6383609056819,-19.4209047482335));
#31961=CARTESIAN_POINT('Ctrl Pts',(-21.0928893911118,25.6353184527499,-19.4211502868506));
#31962=CARTESIAN_POINT('Ctrl Pts',(-21.085530519771,25.6266238149476,-19.4218515448076));
#31963=CARTESIAN_POINT('Ctrl Pts',(-21.080770229043,25.6209600092022,-19.4223078304448));
#31964=CARTESIAN_POINT('Ctrl Pts',(-21.0701212483635,25.6082008789787,-19.4233345811151));
#31965=CARTESIAN_POINT('Ctrl Pts',(-21.0642434393196,25.6010965951066,-19.4239054857318));
#31966=CARTESIAN_POINT('Ctrl Pts',(-20.9266463548883,25.4333275040937,-19.4373694648908));
#31967=CARTESIAN_POINT('Ctrl Pts',(-20.8107647769009,25.260357047993,-19.4509122901936));
#31968=CARTESIAN_POINT('Ctrl Pts',(-20.5774310115296,24.8267721832549,-19.4839319755977));
#31969=CARTESIAN_POINT('Ctrl Pts',(-20.4763280712769,24.5592973509226,-19.5036523149232));
#31970=CARTESIAN_POINT('Ctrl Pts',(-20.4081297605235,24.2667903292781,-19.5226509964112));
#31971=CARTESIAN_POINT('Ctrl Pts',(-20.4046910469264,24.2515405564094,-19.5236340444236));
#31972=CARTESIAN_POINT('Ctrl Pts',(-20.4006099815383,24.2328079466327,-19.5248319845485));
#31973=CARTESIAN_POINT('Ctrl Pts',(-20.3998623057592,24.2293486315534,-19.5250528043334));
#31974=CARTESIAN_POINT('Ctrl Pts',(-20.3986359326965,24.2236288855914,-19.5254172436215));
#31975=CARTESIAN_POINT('Ctrl Pts',(-20.3981539676953,24.2213691713123,-19.5255610504826));
#31976=CARTESIAN_POINT('Ctrl Pts',(-20.3973258924179,24.2174661332563,-19.5258091363349));
#31977=CARTESIAN_POINT('Ctrl Pts',(-20.3969786370743,24.2158230601311,-19.5259134815507));
#31978=CARTESIAN_POINT('Ctrl Pts',(-20.3962015183368,24.2121317861626,-19.5261476925619));
#31979=CARTESIAN_POINT('Ctrl Pts',(-20.3957723663953,24.2100834412098,-19.5262775166999));
#31980=CARTESIAN_POINT('Ctrl Pts',(-20.3946331497376,24.2046194391458,-19.5266234470054));
#31981=CARTESIAN_POINT('Ctrl Pts',(-20.3939266329333,24.2012030324489,-19.5268393484085));
#31982=CARTESIAN_POINT('Ctrl Pts',(-20.3906477388599,24.1852168854184,-19.5278477864977));
#31983=CARTESIAN_POINT('Ctrl Pts',(-20.3881448445428,24.1726327734237,-19.5286363745129));
#31984=CARTESIAN_POINT('Ctrl Pts',(-20.3299439530956,23.87059204003,-19.5474456161531));
#31985=CARTESIAN_POINT('Ctrl Pts',(-20.3141330183758,23.5748105509576,-19.5633537629813));
#31986=CARTESIAN_POINT('Ctrl Pts',(-20.3557014824733,23.0790802370371,-19.5913499418242));
#31987=CARTESIAN_POINT('Ctrl Pts',(-20.3916238208292,22.8792788516211,-19.6029962454273));
#31988=CARTESIAN_POINT('Ctrl Pts',(-20.449407649001,22.6721669400113,-19.6160633649876));
#31989=CARTESIAN_POINT('Ctrl Pts',(-20.4528309957934,22.6601665162353,-19.6168239817271));
#31990=CARTESIAN_POINT('Ctrl Pts',(-20.4576117131381,22.643769494096,-19.6178681402334));
#31991=CARTESIAN_POINT('Ctrl Pts',(-20.4589089607933,22.6393553605794,-19.618149716062));
#31992=CARTESIAN_POINT('Ctrl Pts',(-20.4611355687091,22.631838440731,-19.6186300496754));
#31993=CARTESIAN_POINT('Ctrl Pts',(-20.4620601652255,22.6287342404746,-19.6188286513023));
#31994=CARTESIAN_POINT('Ctrl Pts',(-20.463922233094,22.622516889919,-19.6192269149563));
#31995=CARTESIAN_POINT('Ctrl Pts',(-20.4648597387094,22.6194037545269,-19.6194265778784));
#31996=CARTESIAN_POINT('Ctrl Pts',(-20.4670191236614,22.6122722791442,-19.6198845247216));
#31997=CARTESIAN_POINT('Ctrl Pts',(-20.4682441486332,22.6082549048084,-19.6201429116296));
#31998=CARTESIAN_POINT('Ctrl Pts',(-20.4719391875614,22.5962216764022,-19.6209180984171));
#31999=CARTESIAN_POINT('Ctrl Pts',(-20.4744326316097,22.5882131054614,-19.6214356676769));
#32000=CARTESIAN_POINT('Ctrl Pts',(-20.4801903991027,22.5699712248482,-19.6226183964494));
#32001=CARTESIAN_POINT('Ctrl Pts',(-20.4834746633945,22.5597443588191,-19.6232842093964));
#32002=CARTESIAN_POINT('Ctrl Pts',(-20.4942846670143,22.5266523045667,-19.6254476557528));
#32003=CARTESIAN_POINT('Ctrl Pts',(-20.5020153379869,22.5038553914684,-19.6269520349394));
#32004=CARTESIAN_POINT('Ctrl Pts',(-20.5335662179376,22.4141330136436,-19.6329294339128));
#32005=CARTESIAN_POINT('Ctrl Pts',(-20.5593396127607,22.3479204143598,-19.6374663891675));
#32006=CARTESIAN_POINT('Ctrl Pts',(-20.6467638627611,22.1435746960247,-19.6518715983428));
#32007=CARTESIAN_POINT('Ctrl Pts',(-20.7159568202081,22.0089064204421,-19.6619678131959));
#32008=CARTESIAN_POINT('Ctrl Pts',(-20.9211493835702,21.6704189925308,-19.688694798623));
#32009=CARTESIAN_POINT('Ctrl Pts',(-21.0713743044207,21.4763331640326,-19.7054623361572));
#32010=CARTESIAN_POINT('Ctrl Pts',(-21.2518837759907,21.2910902703407,-19.7217992599717));
#32011=CARTESIAN_POINT('Ctrl Pts',(-21.2617070911371,21.2811397438866,-19.7226777524069));
#32012=CARTESIAN_POINT('Ctrl Pts',(-21.2742308544671,21.2686178589289,-19.7237840774876));
#32013=CARTESIAN_POINT('Ctrl Pts',(-21.2768712283336,21.2659870250077,-19.7240165612863));
#32014=CARTESIAN_POINT('Ctrl Pts',(-21.2810547326442,21.2618330744549,-19.7243837053143));
#32015=CARTESIAN_POINT('Ctrl Pts',(-21.2825948357581,21.2603069346083,-19.7245186058686));
#32016=CARTESIAN_POINT('Ctrl Pts',(-21.2854626190067,21.257470882156,-19.7247693174513));
#32017=CARTESIAN_POINT('Ctrl Pts',(-21.2867898877474,21.2561605761357,-19.7248851597342));
#32018=CARTESIAN_POINT('Ctrl Pts',(-21.2897547532663,21.2532386799526,-19.7251435014887));
#32019=CARTESIAN_POINT('Ctrl Pts',(-21.2913929325571,21.2516276921791,-19.7252859528485));
#32020=CARTESIAN_POINT('Ctrl Pts',(-21.2961928331783,21.2469175497213,-19.7257024944224));
#32021=CARTESIAN_POINT('Ctrl Pts',(-21.2993592359291,21.2438231407764,-19.7259762094056));
#32022=CARTESIAN_POINT('Ctrl Pts',(-21.3225747567711,21.2212288079685,-19.7279753217666));
#32023=CARTESIAN_POINT('Ctrl Pts',(-21.3428713845086,21.2019833022699,-19.7296810737574));
#32024=CARTESIAN_POINT('Ctrl Pts',(-21.4097834998578,21.1401707030678,-19.7351795656534));
#32025=CARTESIAN_POINT('Ctrl Pts',(-21.4574019337613,21.0987061652177,-19.7388997536697));
#32026=CARTESIAN_POINT('Ctrl Pts',(-21.6214472849169,20.9641271242077,-19.7512044792263));
#32027=CARTESIAN_POINT('Ctrl Pts',(-21.7431114300877,20.8776917068828,-19.7595091210275));
#32028=CARTESIAN_POINT('Ctrl Pts',(-22.0285067156216,20.7033660758271,-19.7781954220176));
#32029=CARTESIAN_POINT('Ctrl Pts',(-22.1947100928316,20.6205819871243,-19.7885685731215));
#32030=CARTESIAN_POINT('Ctrl Pts',(-22.3868943477496,20.5447295816147,-19.8006596444988));
#32031=CARTESIAN_POINT('Ctrl Pts',(-22.4067664327626,20.5371129762922,-19.8019106231367));
#32032=CARTESIAN_POINT('Ctrl Pts',(-22.4315551481153,20.5278924562185,-19.8034727619962));
#32033=CARTESIAN_POINT('Ctrl Pts',(-22.4364024158384,20.5261027039184,-19.8037783055445));
#32034=CARTESIAN_POINT('Ctrl Pts',(-22.4449908151605,20.5229550669031,-19.8043198195477));
#32035=CARTESIAN_POINT('Ctrl Pts',(-22.4487302047519,20.5215924376237,-19.8045556454322));
#32036=CARTESIAN_POINT('Ctrl Pts',(-22.4617722117909,20.5168672938779,-19.8053783326243));
#32037=CARTESIAN_POINT('Ctrl Pts',(-22.4710877150946,20.5135407074795,-19.8059662868663));
#32038=CARTESIAN_POINT('Ctrl Pts',(-22.4858110310312,20.5083592828704,-19.8068961662564));
#32039=CARTESIAN_POINT('Ctrl Pts',(-22.4912087645313,20.5064758407729,-19.8072371988405));
#32040=CARTESIAN_POINT('Ctrl Pts',(-22.4982881541329,20.5040267261077,-19.8076846600247));
#32041=CARTESIAN_POINT('Ctrl Pts',(-22.4999653286532,20.5034480579235,-19.8077906810664));
#32042=CARTESIAN_POINT('Ctrl Pts',(-22.508121272378,20.5006415829897,-19.808306317247));
#32043=CARTESIAN_POINT('Ctrl Pts',(-22.5146066216677,20.4984330665099,-19.8087165364357));
#32044=CARTESIAN_POINT('Ctrl Pts',(-22.5268819340266,20.4942964745398,-19.8094933993487));
#32045=CARTESIAN_POINT('Ctrl Pts',(-22.5326704344476,20.4923641298674,-19.8098599057579));
#32046=CARTESIAN_POINT('Ctrl Pts',(-22.56316358176,20.4822809340344,-19.8117915776066));
#32047=CARTESIAN_POINT('Ctrl Pts',(-22.5879602132796,20.4744131743574,-19.8133657065999));
#32048=CARTESIAN_POINT('Ctrl Pts',(-22.6222528684818,20.463987669889,-19.8155482097231));
#32049=CARTESIAN_POINT('Ctrl Pts',(-22.631669851872,20.4611717575642,-19.8161481107525));
#32050=CARTESIAN_POINT('Ctrl Pts',(-22.6453708182116,20.4571430171703,-19.817021797726));
#32051=CARTESIAN_POINT('Ctrl Pts',(-22.6496447290464,20.4558958990922,-19.8172944614795));
#32052=CARTESIAN_POINT('Ctrl Pts',(-22.6571839231105,20.4537129209718,-19.8177756646758));
#32053=CARTESIAN_POINT('Ctrl Pts',(-22.6604481343065,20.4527733574851,-19.8179840827766));
#32054=CARTESIAN_POINT('Ctrl Pts',(-22.6667253928913,20.4509772664725,-19.8183850263193));
#32055=CARTESIAN_POINT('Ctrl Pts',(-22.6697382170709,20.4501199673916,-19.8185775263032));
#32056=CARTESIAN_POINT('Ctrl Pts',(-22.677661233151,20.4478779547492,-19.8190839256426));
#32057=CARTESIAN_POINT('Ctrl Pts',(-22.6825734572458,20.4465005098256,-19.8193980616306));
#32058=CARTESIAN_POINT('Ctrl Pts',(-22.7004368810623,20.441537119292,-19.8205410614067));
#32059=CARTESIAN_POINT('Ctrl Pts',(-22.7134070683091,20.4380205646029,-19.8213721803461));
#32060=CARTESIAN_POINT('Ctrl Pts',(-22.7450293766645,20.4296589016538,-19.82340162249));
#32061=CARTESIAN_POINT('Ctrl Pts',(-22.7637035155375,20.4248998232173,-19.8246027085615));
#32062=CARTESIAN_POINT('Ctrl Pts',(-22.8337093076507,20.4077260963937,-19.8291157250854));
#32063=CARTESIAN_POINT('Ctrl Pts',(-22.8852986427714,20.3964068815349,-19.832462463383));
#32064=CARTESIAN_POINT('Ctrl Pts',(-23.0589403267471,20.3627578748562,-19.8438017704267));
#32065=CARTESIAN_POINT('Ctrl Pts',(-23.1819886790433,20.3462104280648,-19.8519648258069));
#32066=CARTESIAN_POINT('Ctrl Pts',(-23.5617583205988,20.3173057936627,-19.8774395521724));
#32067=CARTESIAN_POINT('Ctrl Pts',(-23.8192478414564,20.3284953991281,-19.8951718110219));
#32068=CARTESIAN_POINT('Ctrl Pts',(-24.0799383857797,20.3713211702789,-19.9123198902541));
#32069=CARTESIAN_POINT('Ctrl Pts',(-24.0871951543888,20.3725388368365,-19.9127965118293));
#32070=CARTESIAN_POINT('Ctrl Pts',(-24.1389999168944,20.3814140643021,-19.9161935552828));
#32071=CARTESIAN_POINT('Ctrl Pts',(-24.1833894759612,20.389983738241,-19.919075473664));
#32072=CARTESIAN_POINT('Ctrl Pts',(-24.2329062909015,20.4006285838789,-19.9222467589812));
#32073=CARTESIAN_POINT('Ctrl Pts',(-24.2382229606921,20.4017856258068,-19.9225866973914));
#32074=CARTESIAN_POINT('Ctrl Pts',(-24.2457692741795,20.4034479223214,-19.92306836645));
#32075=CARTESIAN_POINT('Ctrl Pts',(-24.2480013121186,20.4039420848147,-19.9232107307666));
#32076=CARTESIAN_POINT('Ctrl Pts',(-24.2520916969035,20.4048522431548,-19.9234714331651));
#32077=CARTESIAN_POINT('Ctrl Pts',(-24.2539502035897,20.4052675117625,-19.9235898133965));
#32078=CARTESIAN_POINT('Ctrl Pts',(-24.2577323758251,20.4061161286591,-19.9238305751887));
#32079=CARTESIAN_POINT('Ctrl Pts',(-24.2596560119239,20.4065495951828,-19.9239529496923));
#32080=CARTESIAN_POINT('Ctrl Pts',(-24.2644495779728,20.4076343871742,-19.9242577055948));
#32081=CARTESIAN_POINT('Ctrl Pts',(-24.2673190233495,20.4082878804147,-19.9244399612417));
#32082=CARTESIAN_POINT('Ctrl Pts',(-24.2781296480994,20.4107654947097,-19.9251259729906));
#32083=CARTESIAN_POINT('Ctrl Pts',(-24.2860648832492,20.4126158193451,-19.9256282271659));
#32084=CARTESIAN_POINT('Ctrl Pts',(-24.4298732951135,20.446724386004,-19.9347083925568));
#32085=CARTESIAN_POINT('Ctrl Pts',(-24.5635352286405,20.4877553701181,-19.9427924550898));
#32086=CARTESIAN_POINT('Ctrl Pts',(-24.7975954582408,20.5766181461353,-19.9569846703623));
#32087=CARTESIAN_POINT('Ctrl Pts',(-24.898971945649,20.6212043876961,-19.9631449823489));
#32088=CARTESIAN_POINT('Ctrl Pts',(-25.115644617033,20.730137939894,-19.9767032424342));
#32089=CARTESIAN_POINT('Ctrl Pts',(-25.2296834886624,20.7965264416605,-19.9841022682964));
#32090=CARTESIAN_POINT('Ctrl Pts',(-25.3734690391325,20.8924933821671,-19.9940669678421));
#32091=CARTESIAN_POINT('Ctrl Pts',(-25.4071678481933,20.9159276748197,-19.9964506597254));
#32092=CARTESIAN_POINT('Ctrl Pts',(-25.4565681177933,20.951699764486,-20.0000247535676));
#32093=CARTESIAN_POINT('Ctrl Pts',(-25.4726179534102,20.9635506240094,-20.0011987982374));
#32094=CARTESIAN_POINT('Ctrl Pts',(-25.4926880101929,20.9786598893812,-20.0026838023914));
#32095=CARTESIAN_POINT('Ctrl Pts',(-25.4968120287339,20.9817801393602,-20.0029898495689));
#32096=CARTESIAN_POINT('Ctrl Pts',(-25.5041956509593,20.987394616141,-20.0035394382383));
#32097=CARTESIAN_POINT('Ctrl Pts',(-25.5074580397276,20.9898851737274,-20.0037828473505));
#32098=CARTESIAN_POINT('Ctrl Pts',(-25.5133725791594,20.9944183336544,-20.0042251933871));
#32099=CARTESIAN_POINT('Ctrl Pts',(-25.5160263254498,20.9964588516383,-20.004424054252));
#32100=CARTESIAN_POINT('Ctrl Pts',(-25.5604492198402,21.0307267618891,-20.0077594719829));
#32101=CARTESIAN_POINT('Ctrl Pts',(-25.6014220046944,21.0639693364731,-20.0109332015926));
#32102=CARTESIAN_POINT('Ctrl Pts',(-25.6481957933262,21.103861776483,-20.0146795714722));
#32103=CARTESIAN_POINT('Ctrl Pts',(-25.6548098153013,21.1095492941272,-20.0152122728861));
#32104=CARTESIAN_POINT('Ctrl Pts',(-25.6646391023183,21.1180713369771,-20.0160083821883));
#32105=CARTESIAN_POINT('Ctrl Pts',(-25.667871973619,21.1208855703497,-20.0162709464227));
#32106=CARTESIAN_POINT('Ctrl Pts',(-25.6736308473351,21.1259189332804,-20.0167399609807));
#32107=CARTESIAN_POINT('Ctrl Pts',(-25.6761590139065,21.1281355864409,-20.016946307753));
#32108=CARTESIAN_POINT('Ctrl Pts',(-25.6810395243587,21.1324282622721,-20.0173455197156));
#32109=CARTESIAN_POINT('Ctrl Pts',(-25.6833923156485,21.1345037724241,-20.017538363306));
#32110=CARTESIAN_POINT('Ctrl Pts',(-25.688481870819,21.1390067461524,-20.0179563743439));
#32111=CARTESIAN_POINT('Ctrl Pts',(-25.6912175374457,21.1414354383975,-20.0181815932918));
#32112=CARTESIAN_POINT('Ctrl Pts',(-25.7019722084491,21.1510161009857,-20.0190691092503));
#32113=CARTESIAN_POINT('Ctrl Pts',(-25.709959488574,21.1582034365274,-20.0197328964554));
#32114=CARTESIAN_POINT('Ctrl Pts',(-25.7878670596029,21.229016676879,-20.0262535134748));
#32115=CARTESIAN_POINT('Ctrl Pts',(-25.8549851260073,21.2956440718766,-20.0322387819725));
#32116=CARTESIAN_POINT('Ctrl Pts',(-25.9633729879638,21.4131432674172,-20.0425673365422));
#32117=CARTESIAN_POINT('Ctrl Pts',(-26.0061998656384,21.4625005900652,-20.0468440646524));
#32118=CARTESIAN_POINT('Ctrl Pts',(-26.234049278312,21.7418128355501,-20.0706906139472));
#32119=CARTESIAN_POINT('Ctrl Pts',(-26.3882879258702,21.9950177552171,-20.091191647569));
#32120=CARTESIAN_POINT('Ctrl Pts',(-26.5274473670701,22.3152032224774,-20.1138764610917));
#32121=CARTESIAN_POINT('Ctrl Pts',(-26.5477329248028,22.3652850038846,-20.1173336060852));
#32122=CARTESIAN_POINT('Ctrl Pts',(-26.5685836657827,22.4207296979341,-20.1210438005859));
#32123=CARTESIAN_POINT('Ctrl Pts',(-26.5704044321117,22.4256071803502,-20.1213692038817));
#32124=CARTESIAN_POINT('Ctrl Pts',(-26.573088496102,22.4328507963107,-20.1218509840738));
#32125=CARTESIAN_POINT('Ctrl Pts',(-26.5739608408444,22.4352135336148,-20.1220078987762));
#32126=CARTESIAN_POINT('Ctrl Pts',(-26.5754487451984,22.4392580944012,-20.1222761050777));
#32127=CARTESIAN_POINT('Ctrl Pts',(-26.576065672528,22.4409394078694,-20.1223874789815));
#32128=CARTESIAN_POINT('Ctrl Pts',(-26.577265705739,22.4442183102791,-20.1226044479894));
#32129=CARTESIAN_POINT('Ctrl Pts',(-26.5778489469364,22.4458158421532,-20.1227100508703));
#32130=CARTESIAN_POINT('Ctrl Pts',(-26.5792550493484,22.4496767231417,-20.1229650106527));
#32131=CARTESIAN_POINT('Ctrl Pts',(-26.5800766404044,22.4519405392733,-20.1231142907623));
#32132=CARTESIAN_POINT('Ctrl Pts',(-26.5825858790168,22.4588787500655,-20.1235711572206));
#32133=CARTESIAN_POINT('Ctrl Pts',(-26.5842652626288,22.4635561574379,-20.1238782491583));
#32134=CARTESIAN_POINT('Ctrl Pts',(-26.6017084467488,22.5124944297801,-20.1270819847663));
#32135=CARTESIAN_POINT('Ctrl Pts',(-26.6165143756569,22.5570939559234,-20.1299224801813));
#32136=CARTESIAN_POINT('Ctrl Pts',(-26.6566799556547,22.6875592705903,-20.1380465941811));
#32137=CARTESIAN_POINT('Ctrl Pts',(-26.6794453249952,22.7741816695343,-20.1432114601558));
#32138=CARTESIAN_POINT('Ctrl Pts',(-26.7478922037191,23.0871221436809,-20.1614170461536));
#32139=CARTESIAN_POINT('Ctrl Pts',(-26.7728426734292,23.3172330135266,-20.174018082798));
#32140=CARTESIAN_POINT('Ctrl Pts',(-26.7730017660406,23.5480310413434,-20.1872301387646));
#32141=CARTESIAN_POINT('Ctrl Pts',(-22.0750360153462,26.4155367745563,-20.5963779455771));
#32142=CARTESIAN_POINT('Ctrl Pts',(-22.1638777420742,26.4612777103593,-20.5902262515474));
#32143=CARTESIAN_POINT('Ctrl Pts',(-22.2548169866545,26.5028664262311,-20.5840745575176));
#32144=CARTESIAN_POINT('Ctrl Pts',(-22.3474260531731,26.5401231016468,-20.5779228634878));
#32145=CARTESIAN_POINT('Ctrl Pts',(-22.4401405378047,26.5774221868239,-20.5717641669042));
#32146=CARTESIAN_POINT('Ctrl Pts',(-22.5345282342079,26.6103792283644,-20.5656054703206));
#32147=CARTESIAN_POINT('Ctrl Pts',(-22.6301437886602,26.6388634595212,-20.559446773737));
#32148=CARTESIAN_POINT('Ctrl Pts',(-22.7258238098815,26.6673668955695,-20.5532839247822));
#32149=CARTESIAN_POINT('Ctrl Pts',(-22.822732916224,26.6913914138537,-20.5471210758275));
#32150=CARTESIAN_POINT('Ctrl Pts',(-22.9204149840781,26.7108572564443,-20.5409582268727));
#32151=CARTESIAN_POINT('Ctrl Pts',(-23.0182467023896,26.7303529210106,-20.5347859363369));
#32152=CARTESIAN_POINT('Ctrl Pts',(-23.1168533171266,26.7452759086086,-20.528613645801));
#32153=CARTESIAN_POINT('Ctrl Pts',(-23.2157732093474,26.7555982455638,-20.5224413552651));
#32154=CARTESIAN_POINT('Ctrl Pts',(-23.2433700368798,26.7584779874063,-20.5207193999175));
#32155=CARTESIAN_POINT('Ctrl Pts',(-23.2709912485032,26.7609999694031,-20.5189974445698));
#32156=CARTESIAN_POINT('Ctrl Pts',(-23.2986268448676,26.7631643070514,-20.5172754892222));
#32157=CARTESIAN_POINT('Ctrl Pts',(-23.3976825053207,26.7709220515331,-20.5111033979099));
#32158=CARTESIAN_POINT('Ctrl Pts',(-23.4972717224806,26.7741082642045,-20.5049313065975));
#32159=CARTESIAN_POINT('Ctrl Pts',(-23.5969366756859,26.7726643851356,-20.4987592152852));
#32160=CARTESIAN_POINT('Ctrl Pts',(-23.6964665927324,26.7712224623802,-20.4925954865464));
#32161=CARTESIAN_POINT('Ctrl Pts',(-23.7960716113389,26.7651629230061,-20.4864317578076));
#32162=CARTESIAN_POINT('Ctrl Pts',(-23.8952892272566,26.7544789970389,-20.4802680290689));
#32163=CARTESIAN_POINT('Ctrl Pts',(-23.9944017314228,26.7438063896885,-20.4741108302222));
#32164=CARTESIAN_POINT('Ctrl Pts',(-24.0931272193255,26.7285191818588,-20.4679536313755));
#32165=CARTESIAN_POINT('Ctrl Pts',(-24.1910045961852,26.7086626308344,-20.4617964325288));
#32166=CARTESIAN_POINT('Ctrl Pts',(-24.2888104306174,26.6888205937446,-20.4556437342211));
#32167=CARTESIAN_POINT('Ctrl Pts',(-24.3857689620633,26.6644159398765,-20.4494910359134));
#32168=CARTESIAN_POINT('Ctrl Pts',(-24.4814265383603,26.6355454726982,-20.4433383376057));
#32169=CARTESIAN_POINT('Ctrl Pts',(-24.5770478411683,26.6066859532422,-20.4371879724099));
#32170=CARTESIAN_POINT('Ctrl Pts',(-24.6713687536461,26.5733641107049,-20.4310376072142));
#32171=CARTESIAN_POINT('Ctrl Pts',(-24.7639489711685,26.5357271196462,-20.4248872420184));
#32172=CARTESIAN_POINT('Ctrl Pts',(-24.8565188500734,26.4980943315854,-20.4187375636462));
#32173=CARTESIAN_POINT('Ctrl Pts',(-24.947348018071,26.4561475166455,-20.412587885274));
#32174=CARTESIAN_POINT('Ctrl Pts',(-25.0360153539962,26.4100823165529,-20.4064382069018));
#32175=CARTESIAN_POINT('Ctrl Pts',(-25.1246965091997,26.3640099369527,-20.4002875700694));
#32176=CARTESIAN_POINT('Ctrl Pts',(-25.2112147775757,26.3138180975655,-20.3941369332369));
#32177=CARTESIAN_POINT('Ctrl Pts',(-25.2951737847896,26.2597483119079,-20.3879862964045));
#32178=CARTESIAN_POINT('Ctrl Pts',(-25.3792226105042,26.205620682938,-20.3818290796827));
#32179=CARTESIAN_POINT('Ctrl Pts',(-25.4607063418638,26.1476070590383,-20.3756718629608));
#32180=CARTESIAN_POINT('Ctrl Pts',(-25.539257859553,26.0859921414036,-20.369514646239));
#32181=CARTESIAN_POINT('Ctrl Pts',(-25.6178532008122,26.0243428490588,-20.3633539944312));
#32182=CARTESIAN_POINT('Ctrl Pts',(-25.6935127416238,25.9590885455185,-20.3571933426234));
#32183=CARTESIAN_POINT('Ctrl Pts',(-25.7659043162503,25.890552668876,-20.3510326908156));
#32184=CARTESIAN_POINT('Ctrl Pts',(-25.838417027724,25.8219021073403,-20.3448617300466));
#32185=CARTESIAN_POINT('Ctrl Pts',(-25.9076505485135,25.7499593172403,-20.3386907692775));
#32186=CARTESIAN_POINT('Ctrl Pts',(-25.9733111872545,25.6750829518017,-20.3325198085085));
#32187=CARTESIAN_POINT('Ctrl Pts',(-26.0234311856438,25.6179284161905,-20.3278093982881));
#32188=CARTESIAN_POINT('Ctrl Pts',(-26.0714702194857,25.559065345811,-20.3230989880677));
#32189=CARTESIAN_POINT('Ctrl Pts',(-26.1173147644303,25.4986644634375,-20.3183885778473));
#32190=CARTESIAN_POINT('Ctrl Pts',(-26.1775491597017,25.419304735295,-20.3121996471588));
#32191=CARTESIAN_POINT('Ctrl Pts',(-26.2342080193949,25.3370069965089,-20.3060107164704));
#32192=CARTESIAN_POINT('Ctrl Pts',(-26.2869923957093,25.2521257582334,-20.2998217857819));
#32193=CARTESIAN_POINT('Ctrl Pts',(-26.3397054514696,25.1673592087609,-20.2936412173778));
#32194=CARTESIAN_POINT('Ctrl Pts',(-26.3885542013232,25.0800164585051,-20.2874606489738));
#32195=CARTESIAN_POINT('Ctrl Pts',(-26.4332805275755,24.9904841580185,-20.2812800805697));
#32196=CARTESIAN_POINT('Ctrl Pts',(-26.4779581565968,24.9010493387132,-20.2751062414589));
#32197=CARTESIAN_POINT('Ctrl Pts',(-26.518522092179,24.8094300906717,-20.2689324023481));
#32198=CARTESIAN_POINT('Ctrl Pts',(-26.5547585763202,24.7160402440611,-20.2627585632373));
#32199=CARTESIAN_POINT('Ctrl Pts',(-26.5909645161969,24.6227291171236,-20.2565899281461));
#32200=CARTESIAN_POINT('Ctrl Pts',(-26.6228501031439,24.5276507598022,-20.250421293055));
#32201=CARTESIAN_POINT('Ctrl Pts',(-26.6502488565259,24.4312408111453,-20.2442526579638));
#32202=CARTESIAN_POINT('Ctrl Pts',(-26.6776333669897,24.334880980061,-20.2380872295648));
#32203=CARTESIAN_POINT('Ctrl Pts',(-26.700535564415,24.2371913478903,-20.2319218011657));
#32204=CARTESIAN_POINT('Ctrl Pts',(-26.7188384674342,24.138623783822,-20.2257563727666));
#32205=CARTESIAN_POINT('Ctrl Pts',(-26.7371416973062,24.040054459537,-20.2195908342654));
#32206=CARTESIAN_POINT('Ctrl Pts',(-26.7508453764792,23.9406075932114,-20.2134252957643));
#32207=CARTESIAN_POINT('Ctrl Pts',(-26.7598835437495,23.8407457828255,-20.2072597572632));
#32208=CARTESIAN_POINT('Ctrl Pts',(-26.7686952713363,23.7433858819598,-20.2012486884178));
#32209=CARTESIAN_POINT('Ctrl Pts',(-26.7730725069817,23.6456319789118,-20.1952376195724));
#32210=CARTESIAN_POINT('Ctrl Pts',(-26.7730016852365,23.5479167572311,-20.189226550727));
#32211=CARTESIAN_POINT('',(-26.7730016643153,23.5526169957307,-20.4357734492732));
#32212=CARTESIAN_POINT('Ctrl Pts',(-22.0750362008293,26.4155368700539,-20.8439479435254));
#32213=CARTESIAN_POINT('Ctrl Pts',(-22.1728011864774,26.4658720153252,-20.8377462766994));
#32214=CARTESIAN_POINT('Ctrl Pts',(-22.2731130362056,26.5111884925568,-20.8314660366905));
#32215=CARTESIAN_POINT('Ctrl Pts',(-22.3953000544431,26.5590148235372,-20.823786419488));
#32216=CARTESIAN_POINT('Ctrl Pts',(-22.4150894173956,26.5665367406279,-20.8225418481915));
#32217=CARTESIAN_POINT('Ctrl Pts',(-22.4402142728685,26.5758043980314,-20.8209600092893));
#32218=CARTESIAN_POINT('Ctrl Pts',(-22.4454824364433,26.5777320226312,-20.8206282358822));
#32219=CARTESIAN_POINT('Ctrl Pts',(-22.4545154449924,26.5810104893776,-20.8200591849443));
#32220=CARTESIAN_POINT('Ctrl Pts',(-22.4582778319827,26.5823680994493,-20.8198221134987));
#32221=CARTESIAN_POINT('Ctrl Pts',(-22.467444802669,26.5856566106294,-20.8192443568174));
#32222=CARTESIAN_POINT('Ctrl Pts',(-22.4728520225352,26.5875800811548,-20.8189034456791));
#32223=CARTESIAN_POINT('Ctrl Pts',(-22.4847371184443,26.5917721479415,-20.8181538442351));
#32224=CARTESIAN_POINT('Ctrl Pts',(-22.4912171506158,26.594034510165,-20.8177449636832));
#32225=CARTESIAN_POINT('Ctrl Pts',(-22.5057864918327,26.5990689209045,-20.8168252176098));
#32226=CARTESIAN_POINT('Ctrl Pts',(-22.5138796845367,26.601829501582,-20.8163139983253));
#32227=CARTESIAN_POINT('Ctrl Pts',(-22.5278247006265,26.6065242599274,-20.8154325620961));
#32228=CARTESIAN_POINT('Ctrl Pts',(-22.5336712881877,26.6084739300081,-20.8150628371232));
#32229=CARTESIAN_POINT('Ctrl Pts',(-22.5521150338715,26.6145656591625,-20.8138959138742));
#32230=CARTESIAN_POINT('Ctrl Pts',(-22.5647320687554,26.6186467073016,-20.8130967871932));
#32231=CARTESIAN_POINT('Ctrl Pts',(-22.5973670987757,26.6289806338534,-20.8110273103342));
#32232=CARTESIAN_POINT('Ctrl Pts',(-22.6174213489648,26.6351161149852,-20.8097532256629));
#32233=CARTESIAN_POINT('Ctrl Pts',(-22.6435980254541,26.6428461280065,-20.8080866088396));
#32234=CARTESIAN_POINT('Ctrl Pts',(-22.6496675823347,26.6446190732861,-20.8076999245154));
#32235=CARTESIAN_POINT('Ctrl Pts',(-22.6593673566637,26.6474214656511,-20.8070815542785));
#32236=CARTESIAN_POINT('Ctrl Pts',(-22.6629942538854,26.6484624259435,-20.8068502448462));
#32237=CARTESIAN_POINT('Ctrl Pts',(-22.669526467058,26.6503248336288,-20.8064334785065));
#32238=CARTESIAN_POINT('Ctrl Pts',(-22.6724311293727,26.6511485737564,-20.8062480966874));
#32239=CARTESIAN_POINT('Ctrl Pts',(-22.6784146895188,26.6528363848247,-20.8058660888893));
#32240=CARTESIAN_POINT('Ctrl Pts',(-22.6814937236553,26.6536999570736,-20.805669446869));
#32241=CARTESIAN_POINT('Ctrl Pts',(-22.6907101316287,26.6562700790897,-20.8050806373804));
#32242=CARTESIAN_POINT('Ctrl Pts',(-22.6968512582895,26.6579630085337,-20.804688026764));
#32243=CARTESIAN_POINT('Ctrl Pts',(-22.7264740353126,26.6660347174153,-20.8027928565694));
#32244=CARTESIAN_POINT('Ctrl Pts',(-22.7500219001005,26.6721654907448,-20.8012822608865));
#32245=CARTESIAN_POINT('Ctrl Pts',(-22.8136341204583,26.6879601862086,-20.7971896458651));
#32246=CARTESIAN_POINT('Ctrl Pts',(-22.8538170594614,26.6971229434944,-20.7945917207726));
#32247=CARTESIAN_POINT('Ctrl Pts',(-22.9715958797011,26.72161329674,-20.7869374055628));
#32248=CARTESIAN_POINT('Ctrl Pts',(-23.0495893452092,26.7348572693042,-20.7818181383961));
#32249=CARTESIAN_POINT('Ctrl Pts',(-23.2168930447791,26.7569691619173,-20.7707356370175));
#32250=CARTESIAN_POINT('Ctrl Pts',(-23.3062465495207,26.7650028202297,-20.764755701666));
#32251=CARTESIAN_POINT('Ctrl Pts',(-23.6423057295988,26.7811257644728,-20.7421248145408));
#32252=CARTESIAN_POINT('Ctrl Pts',(-23.8893464196204,26.7646018520771,-20.7251397971366));
#32253=CARTESIAN_POINT('Ctrl Pts',(-24.1672613922096,26.713588823874,-20.7069900151416));
#32254=CARTESIAN_POINT('Ctrl Pts',(-24.202326985266,26.7065471320127,-20.7047193356227));
#32255=CARTESIAN_POINT('Ctrl Pts',(-24.2418072720009,26.6979328159498,-20.7021902556745));
#32256=CARTESIAN_POINT('Ctrl Pts',(-24.2463425686781,26.6969329717431,-20.7019001394121));
#32257=CARTESIAN_POINT('Ctrl Pts',(-24.2531964449155,26.6954064341752,-20.7014623463951));
#32258=CARTESIAN_POINT('Ctrl Pts',(-24.2555166044744,26.6948869783607,-20.701314256522));
#32259=CARTESIAN_POINT('Ctrl Pts',(-24.2595472996977,26.6939798689087,-20.7010571828101));
#32260=CARTESIAN_POINT('Ctrl Pts',(-24.2612580934725,26.6935933865525,-20.7009481312661));
#32261=CARTESIAN_POINT('Ctrl Pts',(-24.2648356490652,26.6927821172494,-20.70072021548));
#32262=CARTESIAN_POINT('Ctrl Pts',(-24.2667023466836,26.6923570637467,-20.7006013673076));
#32263=CARTESIAN_POINT('Ctrl Pts',(-24.271161130064,26.6913376033693,-20.7003176612241));
#32264=CARTESIAN_POINT('Ctrl Pts',(-24.2737528686925,26.6907416492027,-20.7001528930762));
#32265=CARTESIAN_POINT('Ctrl Pts',(-24.2825118407148,26.6887161598126,-20.6995965129649));
#32266=CARTESIAN_POINT('Ctrl Pts',(-24.2886756492856,26.6872716488953,-20.6992057620682));
#32267=CARTESIAN_POINT('Ctrl Pts',(-24.3033008666448,26.6837986820017,-20.6982803752122));
#32268=CARTESIAN_POINT('Ctrl Pts',(-24.3117584462962,26.6817540911566,-20.6977466446204));
#32269=CARTESIAN_POINT('Ctrl Pts',(-24.4105428425839,26.6574494290197,-20.691528060085));
#32270=CARTESIAN_POINT('Ctrl Pts',(-24.4998829263389,26.6313201566784,-20.6860541746404));
#32271=CARTESIAN_POINT('Ctrl Pts',(-24.7138612024888,26.5585431990297,-20.6730351439377));
#32272=CARTESIAN_POINT('Ctrl Pts',(-24.8369832640881,26.5079756012638,-20.6656185777861));
#32273=CARTESIAN_POINT('Ctrl Pts',(-25.0159081157461,26.4211950756656,-20.6545073286861));
#32274=CARTESIAN_POINT('Ctrl Pts',(-25.0742856695943,26.3906363450886,-20.6508266112345));
#32275=CARTESIAN_POINT('Ctrl Pts',(-25.2109697327046,26.3136590796689,-20.6420021301325));
#32276=CARTESIAN_POINT('Ctrl Pts',(-25.2883242426479,26.2656719677553,-20.6368389076801));
#32277=CARTESIAN_POINT('Ctrl Pts',(-25.4596775539725,26.1490478180627,-20.624859523605));
#32278=CARTESIAN_POINT('Ctrl Pts',(-25.5521914651937,26.0784686239829,-20.6179901499027));
#32279=CARTESIAN_POINT('Ctrl Pts',(-25.6487442819638,25.9961801944573,-20.6102706684643));
#32280=CARTESIAN_POINT('Ctrl Pts',(-25.6567718942425,25.9892699421326,-20.6096245169186));
#32281=CARTESIAN_POINT('Ctrl Pts',(-25.6680023711404,25.9795058285841,-20.6087143845018));
#32282=CARTESIAN_POINT('Ctrl Pts',(-25.6712338874162,25.9766849027516,-20.6084517739132));
#32283=CARTESIAN_POINT('Ctrl Pts',(-25.6768334831204,25.9717770479041,-20.6079954562565));
#32284=CARTESIAN_POINT('Ctrl Pts',(-25.6792041522966,25.9696930708689,-20.6078018726408));
#32285=CARTESIAN_POINT('Ctrl Pts',(-25.6839683569311,25.9654925918635,-20.6074120403205));
#32286=CARTESIAN_POINT('Ctrl Pts',(-25.6863618136091,25.9633760069261,-20.6072157882734));
#32287=CARTESIAN_POINT('Ctrl Pts',(-25.6912358597575,25.9590528500609,-20.6068153070132));
#32288=CARTESIAN_POINT('Ctrl Pts',(-25.6937161942924,25.9568459979444,-20.6066110661496));
#32289=CARTESIAN_POINT('Ctrl Pts',(-25.7018764469939,25.949562874211,-20.605937657493));
#32290=CARTESIAN_POINT('Ctrl Pts',(-25.7075417447434,25.9444703251003,-20.6054678033207));
#32291=CARTESIAN_POINT('Ctrl Pts',(-25.7453762986048,25.9102174462648,-20.6023141873179));
#32292=CARTESIAN_POINT('Ctrl Pts',(-25.7769701735555,25.8804308501906,-20.5996038495936));
#32293=CARTESIAN_POINT('Ctrl Pts',(-25.8646841965859,25.7943211959147,-20.5918526594682));
#32294=CARTESIAN_POINT('Ctrl Pts',(-25.9193322750013,25.736550206616,-20.5867491694219));
#32295=CARTESIAN_POINT('Ctrl Pts',(-26.0046111093449,25.6394428677489,-20.5783217624909));
#32296=CARTESIAN_POINT('Ctrl Pts',(-26.0365658478906,25.6013103125668,-20.5750479017174));
#32297=CARTESIAN_POINT('Ctrl Pts',(-26.2581846089199,25.324053512358,-20.5515095091151));
#32298=CARTESIAN_POINT('Ctrl Pts',(-26.4138994550013,25.0598148845557,-20.5302607346492));
#32299=CARTESIAN_POINT('Ctrl Pts',(-26.5441958444199,24.7434774216934,-20.5082673758524));
#32300=CARTESIAN_POINT('Ctrl Pts',(-26.5576772209766,24.7090791917104,-20.5059205628949));
#32301=CARTESIAN_POINT('Ctrl Pts',(-26.5723581623587,24.6696369824769,-20.5032863829817));
#32302=CARTESIAN_POINT('Ctrl Pts',(-26.5741399697726,24.6648146673562,-20.5029652795554));
#32303=CARTESIAN_POINT('Ctrl Pts',(-26.5767546689224,24.6576857754895,-20.5024920250336));
#32304=CARTESIAN_POINT('Ctrl Pts',(-26.5775964681088,24.6553825090545,-20.5023393428675));
#32305=CARTESIAN_POINT('Ctrl Pts',(-26.579081250292,24.6513055346493,-20.5020694766608));
#32306=CARTESIAN_POINT('Ctrl Pts',(-26.5797253051365,24.6495322217483,-20.5019522279953));
#32307=CARTESIAN_POINT('Ctrl Pts',(-26.5810661292679,24.6458303263405,-20.5017077405588));
#32308=CARTESIAN_POINT('Ctrl Pts',(-26.581762613718,24.6439016481864,-20.5015805191754));
#32309=CARTESIAN_POINT('Ctrl Pts',(-26.5835750936215,24.6388675631667,-20.5012488594026));
#32310=CARTESIAN_POINT('Ctrl Pts',(-26.5846881648032,24.635761094625,-20.5010445968256));
#32311=CARTESIAN_POINT('Ctrl Pts',(-26.589489014007,24.6222973255368,-20.5001610117546));
#32312=CARTESIAN_POINT('Ctrl Pts',(-26.5931286070458,24.6119227411936,-20.4994845421618));
#32313=CARTESIAN_POINT('Ctrl Pts',(-26.6190264814844,24.5368741069226,-20.4946212373618));
#32314=CARTESIAN_POINT('Ctrl Pts',(-26.6392758342009,24.4715192153636,-20.4905476198389));
#32315=CARTESIAN_POINT('Ctrl Pts',(-26.7339273442685,24.1276688725295,-20.4697100781083));
#32316=CARTESIAN_POINT('Ctrl Pts',(-26.7728002853682,23.840763589504,-20.45422022849));
#32317=CARTESIAN_POINT('Ctrl Pts',(-26.7730017446375,23.5525048579221,-20.4377341936612));
#32318=CARTESIAN_POINT('Ctrl Pts',(-26.7730016643153,23.5526169957307,-20.4357734492732));
#32319=CARTESIAN_POINT('Ctrl Pts',(-26.773075151987,23.4524537761962,-20.4296113721848));
#32320=CARTESIAN_POINT('Ctrl Pts',(-26.7684747048648,23.35224768617,-20.4234492950963));
#32321=CARTESIAN_POINT('Ctrl Pts',(-26.7592150105535,23.2524650709557,-20.4172872180079));
#32322=CARTESIAN_POINT('Ctrl Pts',(-26.7499560101931,23.152689933767,-20.411125602725));
#32323=CARTESIAN_POINT('Ctrl Pts',(-26.7360384965427,23.0533386380498,-20.4049639874422));
#32324=CARTESIAN_POINT('Ctrl Pts',(-26.7175290969173,22.9548730544796,-20.3988023721593));
#32325=CARTESIAN_POINT('Ctrl Pts',(-26.6990162147105,22.8563889444077,-20.3926395975559));
#32326=CARTESIAN_POINT('Ctrl Pts',(-26.6759098092089,22.7587913018524,-20.3864768229525));
#32327=CARTESIAN_POINT('Ctrl Pts',(-26.6483275643628,22.662531486289,-20.3803140483491));
#32328=CARTESIAN_POINT('Ctrl Pts',(-26.6206478325784,22.5659314491534,-20.3741294919788));
#32329=CARTESIAN_POINT('Ctrl Pts',(-26.5884606872596,22.4706791326,-20.3679449356084));
#32330=CARTESIAN_POINT('Ctrl Pts',(-26.5519348922841,22.3772135005348,-20.3617603792381));
#32331=CARTESIAN_POINT('Ctrl Pts',(-26.5154740447795,22.2839140621532,-20.3555868197891));
#32332=CARTESIAN_POINT('Ctrl Pts',(-26.474690179984,22.1923953376775,-20.3494132603401));
#32333=CARTESIAN_POINT('Ctrl Pts',(-26.4297981252393,22.1030708785507,-20.3432397008912));
#32334=CARTESIAN_POINT('Ctrl Pts',(-26.3847861216062,22.0135077498055,-20.3370496460602));
#32335=CARTESIAN_POINT('Ctrl Pts',(-26.3356441787839,21.9261509953061,-20.3308595912292));
#32336=CARTESIAN_POINT('Ctrl Pts',(-26.2826327711642,21.8413886431841,-20.3246695363982));
#32337=CARTESIAN_POINT('Ctrl Pts',(-26.2296213635445,21.7566262910621,-20.3184794815671));
#32338=CARTESIAN_POINT('Ctrl Pts',(-26.1727407892357,21.6744586579882,-20.3122894267362));
#32339=CARTESIAN_POINT('Ctrl Pts',(-26.1122913561492,21.5952398400511,-20.3060993719051));
#32340=CARTESIAN_POINT('Ctrl Pts',(-26.0520173471179,21.5162509148622,-20.2999272805928));
#32341=CARTESIAN_POINT('Ctrl Pts',(-25.9879808586206,21.4399129016145,-20.2937551892805));
#32342=CARTESIAN_POINT('Ctrl Pts',(-25.920443548776,21.366606016105,-20.2875830979682));
#32343=CARTESIAN_POINT('Ctrl Pts',(-25.8529977453093,21.2933984541781,-20.2814193692294));
#32344=CARTESIAN_POINT('Ctrl Pts',(-25.7820608399872,21.2232141737987,-20.2752556404906));
#32345=CARTESIAN_POINT('Ctrl Pts',(-25.7079362077355,21.1564023449355,-20.2690919117518));
#32346=CARTESIAN_POINT('Ctrl Pts',(-25.6338901035747,21.0896612969342,-20.2629347129051));
#32347=CARTESIAN_POINT('Ctrl Pts',(-25.5566633073516,21.0262858866402,-20.2567775140585));
#32348=CARTESIAN_POINT('Ctrl Pts',(-25.4765970244963,20.9665895394386,-20.2506203152118));
#32349=CARTESIAN_POINT('Ctrl Pts',(-25.3965892652386,20.9069368266469,-20.2444676169041));
#32350=CARTESIAN_POINT('Ctrl Pts',(-25.3137464929835,20.8509580892937,-20.2383149185964));
#32351=CARTESIAN_POINT('Ctrl Pts',(-25.2284433619803,20.7989268331184,-20.2321622202887));
#32352=CARTESIAN_POINT('Ctrl Pts',(-25.1431725780458,20.7469153072695,-20.2260118550929));
#32353=CARTESIAN_POINT('Ctrl Pts',(-25.0554436596131,20.6988485142483,-20.2198614898972));
#32354=CARTESIAN_POINT('Ctrl Pts',(-24.9656598963966,20.6549564234444,-20.2137111247014));
#32355=CARTESIAN_POINT('Ctrl Pts',(-24.8758861595119,20.6110692341579,-20.2075614463292));
#32356=CARTESIAN_POINT('Ctrl Pts',(-24.7840584243222,20.5713560110114,-20.201411767957));
#32357=CARTESIAN_POINT('Ctrl Pts',(-24.6906033055421,20.536000107778,-20.1952620895848));
#32358=CARTESIAN_POINT('Ctrl Pts',(-24.5971336212825,20.5006386941383,-20.1891114527524));
#32359=CARTESIAN_POINT('Ctrl Pts',(-24.5020364559823,20.469636103026,-20.1829608159199));
#32360=CARTESIAN_POINT('Ctrl Pts',(-24.4057561053769,20.4431266575275,-20.1768101790875));
#32361=CARTESIAN_POINT('Ctrl Pts',(-24.3093727550212,20.4165888524909,-20.1706529623657));
#32362=CARTESIAN_POINT('Ctrl Pts',(-24.211804111398,20.3945539071583,-20.1644957456439));
#32363=CARTESIAN_POINT('Ctrl Pts',(-24.1135071448038,20.377105544347,-20.1583385289221));
#32364=CARTESIAN_POINT('Ctrl Pts',(-24.0151553387346,20.3596474471655,-20.1521778771142));
#32365=CARTESIAN_POINT('Ctrl Pts',(-23.9160748312988,20.3467810843303,-20.1460172253064));
#32366=CARTESIAN_POINT('Ctrl Pts',(-23.816728150589,20.3385382998494,-20.1398565734986));
#32367=CARTESIAN_POINT('Ctrl Pts',(-23.7172152275543,20.3302817222589,-20.1336856127296));
#32368=CARTESIAN_POINT('Ctrl Pts',(-23.617435675889,20.3266641930229,-20.1275146519606));
#32369=CARTESIAN_POINT('Ctrl Pts',(-23.5178526092488,20.3276654021466,-20.1213436911915));
#32370=CARTESIAN_POINT('Ctrl Pts',(-23.4418389847191,20.3284296438694,-20.1166332809711));
#32371=CARTESIAN_POINT('Ctrl Pts',(-23.3659398565144,20.3318839404417,-20.1119228707507));
#32372=CARTESIAN_POINT('Ctrl Pts',(-23.2903581496809,20.3379990434561,-20.1072124605302));
#32373=CARTESIAN_POINT('Ctrl Pts',(-23.1913227845457,20.3460117159035,-20.1010403692179));
#32374=CARTESIAN_POINT('Ctrl Pts',(-23.09248389645,20.3586227557379,-20.0948682779056));
#32375=CARTESIAN_POINT('Ctrl Pts',(-22.994302804629,20.3758175483505,-20.0886961865933));
#32376=CARTESIAN_POINT('Ctrl Pts',(-22.8962547384809,20.3929890437191,-20.0825324578545));
#32377=CARTESIAN_POINT('Ctrl Pts',(-22.7988631212729,20.4147318734957,-20.0763687291157));
#32378=CARTESIAN_POINT('Ctrl Pts',(-22.7025857025666,20.4409795444355,-20.0702050003769));
#32379=CARTESIAN_POINT('Ctrl Pts',(-22.6064102807493,20.4671994084313,-20.0640478015302));
#32380=CARTESIAN_POINT('Ctrl Pts',(-22.5113471275059,20.4979145118858,-20.0578906026835));
#32381=CARTESIAN_POINT('Ctrl Pts',(-22.4178443688714,20.5330072126536,-20.0517334038368));
#32382=CARTESIAN_POINT('Ctrl Pts',(-22.3244099550834,20.5680742627852,-20.0455807055291));
#32383=CARTESIAN_POINT('Ctrl Pts',(-22.2325340737648,20.6075123963934,-20.0394280072214));
#32384=CARTESIAN_POINT('Ctrl Pts',(-22.1426493463878,20.6511542520191,-20.0332753089137));
#32385=CARTESIAN_POINT('Ctrl Pts',(-22.0527987034272,20.6947795585911,-20.027124943718));
#32386=CARTESIAN_POINT('Ctrl Pts',(-21.9649381044761,20.7426052302821,-20.0209745785222));
#32387=CARTESIAN_POINT('Ctrl Pts',(-21.8794790218281,20.794416280893,-20.0148242133265));
#32388=CARTESIAN_POINT('Ctrl Pts',(-21.7940294825662,20.8462215456607,-20.0086745349543));
#32389=CARTESIAN_POINT('Ctrl Pts',(-21.7109812978908,20.9020110793106,-20.0025248565821));
#32390=CARTESIAN_POINT('Ctrl Pts',(-21.630719329746,20.9615250742127,-19.9963751782098));
#32391=CARTESIAN_POINT('Ctrl Pts',(-21.5504448523447,21.0210483446889,-19.9902245413774));
#32392=CARTESIAN_POINT('Ctrl Pts',(-21.472957802973,21.0842969706306,-19.984073904545));
#32393=CARTESIAN_POINT('Ctrl Pts',(-21.398611350577,21.1509697659034,-19.9779232677125));
#32394=CARTESIAN_POINT('Ctrl Pts',(-21.3241853630945,21.2177138870616,-19.9717660509907));
#32395=CARTESIAN_POINT('Ctrl Pts',(-21.2529070057718,21.2878892018926,-19.9656088342689));
#32396=CARTESIAN_POINT('Ctrl Pts',(-21.1850937278375,21.361156509351,-19.9594516175471));
#32397=CARTESIAN_POINT('Ctrl Pts',(-21.1172426171531,21.43446469234,-19.9532909657393));
#32398=CARTESIAN_POINT('Ctrl Pts',(-21.052860715635,21.5108679710866,-19.9471303139315));
#32399=CARTESIAN_POINT('Ctrl Pts',(-20.9922248302234,21.5899944259826,-19.9409696621237));
#32400=CARTESIAN_POINT('Ctrl Pts',(-20.9314874794131,21.6692532875753,-19.9347987013546));
#32401=CARTESIAN_POINT('Ctrl Pts',(-20.8745089137407,21.7512440706073,-19.9286277405856));
#32402=CARTESIAN_POINT('Ctrl Pts',(-20.8215223786301,21.8355661713767,-19.9224567798166));
#32403=CARTESIAN_POINT('Ctrl Pts',(-20.7810767615102,21.8999308141175,-19.9177463695962));
#32404=CARTESIAN_POINT('Ctrl Pts',(-20.742956222787,21.9656532178648,-19.9130359593758));
#32405=CARTESIAN_POINT('Ctrl Pts',(-20.7072458448747,22.0325468483683,-19.9083255491555));
#32406=CARTESIAN_POINT('Ctrl Pts',(-20.6604542273806,22.1201981518354,-19.9021534578431));
#32407=CARTESIAN_POINT('Ctrl Pts',(-20.6176374976908,22.2101697683839,-19.8959813665308));
#32408=CARTESIAN_POINT('Ctrl Pts',(-20.5790327228931,22.3020656825856,-19.8898092752185));
#32409=CARTESIAN_POINT('Ctrl Pts',(-20.5404802537487,22.3938370869085,-19.8836455464798));
#32410=CARTESIAN_POINT('Ctrl Pts',(-20.5061285634217,22.4875272097641,-19.877481817741));
#32411=CARTESIAN_POINT('Ctrl Pts',(-20.4761691430729,22.5827149963485,-19.8713180890022));
#32412=CARTESIAN_POINT('Ctrl Pts',(-20.4462414619181,22.6778019404071,-19.8651608901555));
#32413=CARTESIAN_POINT('Ctrl Pts',(-20.4206969294587,22.7743829817467,-19.8590036913088));
#32414=CARTESIAN_POINT('Ctrl Pts',(-20.3996788025033,22.8720175138486,-19.8528464924621));
#32415=CARTESIAN_POINT('Ctrl Pts',(-20.3786760385242,22.969580681028,-19.8466937941544));
#32416=CARTESIAN_POINT('Ctrl Pts',(-20.3621931932836,23.0681953846139,-19.8405410958467));
#32417=CARTESIAN_POINT('Ctrl Pts',(-20.3503233130239,23.1674071869397,-19.834388397539));
#32418=CARTESIAN_POINT('Ctrl Pts',(-20.3384579338397,23.2665813680089,-19.8282380323433));
#32419=CARTESIAN_POINT('Ctrl Pts',(-20.331202095456,23.3663517670764,-19.8220876671475));
#32420=CARTESIAN_POINT('Ctrl Pts',(-20.3285973445946,23.4662559964432,-19.8159373019518));
#32421=CARTESIAN_POINT('Ctrl Pts',(-20.3259928846109,23.5661490693058,-19.8097876235796));
#32422=CARTESIAN_POINT('Ctrl Pts',(-20.3280384908415,23.6661755085001,-19.8036379452074));
#32423=CARTESIAN_POINT('Ctrl Pts',(-20.3347236169645,23.7658710861774,-19.7974882668351));
#32424=CARTESIAN_POINT('Ctrl Pts',(-20.3414097850002,23.8655822019431,-19.7913376300027));
#32425=CARTESIAN_POINT('Ctrl Pts',(-20.3527368801113,23.9649619202974,-19.7851869931702));
#32426=CARTESIAN_POINT('Ctrl Pts',(-20.368642412137,24.0635503104069,-19.7790363563378));
#32427=CARTESIAN_POINT('Ctrl Pts',(-20.3845649597408,24.1622441693835,-19.772879139616));
#32428=CARTESIAN_POINT('Ctrl Pts',(-20.4050756556899,24.260144579934,-19.7667219228942));
#32429=CARTESIAN_POINT('Ctrl Pts',(-20.4300607192191,24.356801114151,-19.7605647061723));
#32430=CARTESIAN_POINT('Ctrl Pts',(-20.4550597218129,24.4535115726526,-19.7544040543645));
#32431=CARTESIAN_POINT('Ctrl Pts',(-20.4845379350223,24.5489763577428,-19.7482434025567));
#32432=CARTESIAN_POINT('Ctrl Pts',(-20.5183320825269,24.6427615487833,-19.7420827507489));
#32433=CARTESIAN_POINT('Ctrl Pts',(-20.5521827796576,24.7367036757989,-19.7359117899799));
#32434=CARTESIAN_POINT('Ctrl Pts',(-20.5903636708451,24.8289601931645,-19.7297408292109));
#32435=CARTESIAN_POINT('Ctrl Pts',(-20.6326638005135,24.9191183243077,-19.7235698684418));
#32436=CARTESIAN_POINT('Ctrl Pts',(-20.6649522837129,24.9879377186105,-19.7188594582214));
#32437=CARTESIAN_POINT('Ctrl Pts',(-20.6996398774685,25.055534912831,-19.7141490480009));
#32438=CARTESIAN_POINT('Ctrl Pts',(-20.7366156380375,25.1217374960365,-19.7094386377805));
#32439=CARTESIAN_POINT('Ctrl Pts',(-20.7850601153911,25.2084740362317,-19.7032672066121));
#32440=CARTESIAN_POINT('Ctrl Pts',(-20.8376044284376,25.2931211116169,-19.6970957754438));
#32441=CARTESIAN_POINT('Ctrl Pts',(-20.894043615899,25.3752653421013,-19.6909243442754));
#32442=CARTESIAN_POINT('Ctrl Pts',(-20.9504102682931,25.4573040016598,-19.6847608445673));
#32443=CARTESIAN_POINT('Ctrl Pts',(-21.0106616052613,25.5368458529681,-19.6785973448593));
#32444=CARTESIAN_POINT('Ctrl Pts',(-21.0745469290363,25.6135022333707,-19.6724338451512));
#32445=CARTESIAN_POINT('Ctrl Pts',(-21.1383672489474,25.69008061525,-19.6662766168569));
#32446=CARTESIAN_POINT('Ctrl Pts',(-21.2058139297149,25.7637790299982,-19.6601193885625));
#32447=CARTESIAN_POINT('Ctrl Pts',(-21.2765937197516,25.8342387771378,-19.6539621602682));
#32448=CARTESIAN_POINT('Ctrl Pts',(-21.347318687336,25.9046439497143,-19.647809701052));
#32449=CARTESIAN_POINT('Ctrl Pts',(-21.421371322735,25.9718151382193,-19.6416572418359));
#32450=CARTESIAN_POINT('Ctrl Pts',(-21.4984196399852,26.0354284504173,-19.6355047826197));
#32451=CARTESIAN_POINT('Ctrl Pts',(-21.5754338373058,26.0990135922177,-19.6293550479469));
#32452=CARTESIAN_POINT('Ctrl Pts',(-21.6554407433668,26.1590437153627,-19.623205313274));
#32453=CARTESIAN_POINT('Ctrl Pts',(-21.7380739215636,26.2152340039535,-19.6170555786012));
#32454=CARTESIAN_POINT('Ctrl Pts',(-21.8207025318221,26.2714211863612,-19.6109061838839));
#32455=CARTESIAN_POINT('Ctrl Pts',(-21.9059567684882,26.3237687090981,-19.6047567891666));
#32456=CARTESIAN_POINT('Ctrl Pts',(-21.993440431219,26.3720345300623,-19.5986073944493));
#32457=CARTESIAN_POINT('Ctrl Pts',(-22.0204309851315,26.3869255531653,-19.5967101765635));
#32458=CARTESIAN_POINT('Ctrl Pts',(-22.0476335546389,26.4014283792986,-19.5948129586777));
#32459=CARTESIAN_POINT('Ctrl Pts',(-22.075036015346,26.4155367745563,-19.592915740792));
#32460=CARTESIAN_POINT('Origin',(-23.5502525316942,23.5502525316942,-77.3107734492734));
#32461=CARTESIAN_POINT('',(-22.0750358296283,26.4155366789378,-18.0972636326348));
#32462=CARTESIAN_POINT('',(-22.0750360259987,26.4155367800409,-18.341133076278));
#32463=CARTESIAN_POINT('',(-22.0750360153461,26.4155367745563,-77.3107734492734));
#32464=CARTESIAN_POINT('Ctrl Pts',(-22.0750358296283,26.4155366789378,-18.0972636326348));
#32465=CARTESIAN_POINT('Ctrl Pts',(-22.0020986630162,26.377984338277,-18.102806008076));
#32466=CARTESIAN_POINT('Ctrl Pts',(-21.9305937987179,26.3376462382369,-18.1083246445035));
#32467=CARTESIAN_POINT('Ctrl Pts',(-21.8038493267266,26.2596154407692,-18.1181781376872));
#32468=CARTESIAN_POINT('Ctrl Pts',(-21.7481143339664,26.2228674993881,-18.1225375247352));
#32469=CARTESIAN_POINT('Ctrl Pts',(-21.670171863103,26.1679295164869,-18.1286294835558));
#32470=CARTESIAN_POINT('Ctrl Pts',(-21.6470062787083,26.1511350659498,-18.1304394755775));
#32471=CARTESIAN_POINT('Ctrl Pts',(-21.6205071235855,26.1313801790844,-18.1325062873023));
#32472=CARTESIAN_POINT('Ctrl Pts',(-21.6169532444161,26.1287193510681,-18.1327833966795));
#32473=CARTESIAN_POINT('Ctrl Pts',(-21.6115512989377,26.1246574087145,-18.1332044751031));
#32474=CARTESIAN_POINT('Ctrl Pts',(-21.6096992461742,26.1232616429988,-18.1333488178742));
#32475=CARTESIAN_POINT('Ctrl Pts',(-21.606359336024,26.1207389234167,-18.1336090740878));
#32476=CARTESIAN_POINT('Ctrl Pts',(-21.6048709548795,26.119612679056,-18.1337250370098));
#32477=CARTESIAN_POINT('Ctrl Pts',(-21.601891129799,26.117353799138,-18.1339571683571));
#32478=CARTESIAN_POINT('Ctrl Pts',(-21.6003997007127,26.1162211611328,-18.1340733357544));
#32479=CARTESIAN_POINT('Ctrl Pts',(-21.5961765344237,26.1130081481537,-18.1344022342692));
#32480=CARTESIAN_POINT('Ctrl Pts',(-21.5934471230568,26.1109246984879,-18.134614747664));
#32481=CARTESIAN_POINT('Ctrl Pts',(-21.5820171355823,26.1021708653282,-18.1355044982852));
#32482=CARTESIAN_POINT('Ctrl Pts',(-21.5733471632337,26.0954603676825,-18.1361789268954));
#32483=CARTESIAN_POINT('Ctrl Pts',(-21.4281818613913,25.9819141815755,-18.1474664078731));
#32484=CARTESIAN_POINT('Ctrl Pts',(-21.3004679833139,25.8642642891345,-18.1573323739583));
#32485=CARTESIAN_POINT('Ctrl Pts',(-21.0682662590245,25.6128645685548,-18.1765489436329));
#32486=CARTESIAN_POINT('Ctrl Pts',(-20.9636349811097,25.4800279033554,-18.185882145641));
#32487=CARTESIAN_POINT('Ctrl Pts',(-20.8067748497906,25.2450595326062,-18.2019678016775));
#32488=CARTESIAN_POINT('Ctrl Pts',(-20.7487093743279,25.1472474376841,-18.208551885238));
#32489=CARTESIAN_POINT('Ctrl Pts',(-20.6726468593584,25.0021544072442,-18.2183081332504));
#32490=CARTESIAN_POINT('Ctrl Pts',(-20.650399470392,24.9571943414834,-18.2213292895717));
#32491=CARTESIAN_POINT('Ctrl Pts',(-20.6258784175525,24.9045847803885,-18.2248685794831));
#32492=CARTESIAN_POINT('Ctrl Pts',(-20.6225719084987,24.8974221446742,-18.2253505263329));
#32493=CARTESIAN_POINT('Ctrl Pts',(-20.6175622636763,24.8864645866742,-18.2260879719957));
#32494=CARTESIAN_POINT('Ctrl Pts',(-20.6158401039702,24.8826783524294,-18.226342813992));
#32495=CARTESIAN_POINT('Ctrl Pts',(-20.6128756735162,24.8761273157195,-18.2267837999672));
#32496=CARTESIAN_POINT('Ctrl Pts',(-20.611629961403,24.8733640686204,-18.2269698251464));
#32497=CARTESIAN_POINT('Ctrl Pts',(-20.609058301373,24.8676380478646,-18.2273553427459));
#32498=CARTESIAN_POINT('Ctrl Pts',(-20.6077329280414,24.8646750211089,-18.2275548546781));
#32499=CARTESIAN_POINT('Ctrl Pts',(-20.6045294415223,24.8574841258487,-18.2280390945077));
#32500=CARTESIAN_POINT('Ctrl Pts',(-20.6026559549719,24.8532542144542,-18.2283239809441));
#32501=CARTESIAN_POINT('Ctrl Pts',(-20.5956963639405,24.8374492011152,-18.2293886206598));
#32502=CARTESIAN_POINT('Ctrl Pts',(-20.5906693333279,24.8258483527939,-18.2301703944077));
#32503=CARTESIAN_POINT('Ctrl Pts',(-20.5048355749253,24.6245313883292,-18.243743658637));
#32504=CARTESIAN_POINT('Ctrl Pts',(-20.4423683425129,24.4275585491703,-18.2571737445082));
#32505=CARTESIAN_POINT('Ctrl Pts',(-20.3618196484221,24.051950741957,-18.2829206116642));
#32506=CARTESIAN_POINT('Ctrl Pts',(-20.3389799904374,23.8751095567697,-18.2950839985776));
#32507=CARTESIAN_POINT('Ctrl Pts',(-20.3266631055028,23.605430093448,-18.3131304331952));
#32508=CARTESIAN_POINT('Ctrl Pts',(-20.3264007874225,23.5134243435429,-18.3191945238189));
#32509=CARTESIAN_POINT('Ctrl Pts',(-20.3313362401963,23.3899608836843,-18.3271050704948));
#32510=CARTESIAN_POINT('Ctrl Pts',(-20.3330621556767,23.3584146455631,-18.3291062369557));
#32511=CARTESIAN_POINT('Ctrl Pts',(-20.3355669769764,23.322359935849,-18.3313665519523));
#32512=CARTESIAN_POINT('Ctrl Pts',(-20.3358918191513,23.317823055899,-18.3316504875094));
#32513=CARTESIAN_POINT('Ctrl Pts',(-20.3363984765793,23.3109511314928,-18.3320798055029));
#32514=CARTESIAN_POINT('Ctrl Pts',(-20.3365732322871,23.3086155966791,-18.3322255842483));
#32515=CARTESIAN_POINT('Ctrl Pts',(-20.3368785532151,23.3045940357584,-18.3324763712541));
#32516=CARTESIAN_POINT('Ctrl Pts',(-20.3370078993699,23.3029079237434,-18.332581448628));
#32517=CARTESIAN_POINT('Ctrl Pts',(-20.3372789520385,23.2994106707504,-18.3327992501669));
#32518=CARTESIAN_POINT('Ctrl Pts',(-20.3374208624473,23.2975995525102,-18.3329119623605));
#32519=CARTESIAN_POINT('Ctrl Pts',(-20.3378134090581,23.2926435274327,-18.3332201752954));
#32520=CARTESIAN_POINT('Ctrl Pts',(-20.3380671328196,23.2894988564007,-18.3334155009554));
#32521=CARTESIAN_POINT('Ctrl Pts',(-20.3390535923024,23.2774925657636,-18.334160351134));
#32522=CARTESIAN_POINT('Ctrl Pts',(-20.3398183928529,23.2686335125753,-18.3347080810222));
#32523=CARTESIAN_POINT('Ctrl Pts',(-20.3531492734833,23.1213325664763,-18.3437858295871));
#32524=CARTESIAN_POINT('Ctrl Pts',(-20.3746250627678,22.9838228441027,-18.3518296007611));
#32525=CARTESIAN_POINT('Ctrl Pts',(-20.4493581744545,22.6490452192847,-18.3712707417994));
#32526=CARTESIAN_POINT('Ctrl Pts',(-20.5125940193044,22.4546457854139,-18.3824594673435));
#32527=CARTESIAN_POINT('Ctrl Pts',(-20.6239302144503,22.1980347164166,-18.3983771671318));
#32528=CARTESIAN_POINT('Ctrl Pts',(-20.6565186569245,22.1296334601545,-18.4027361683782));
#32529=CARTESIAN_POINT('Ctrl Pts',(-20.7318549960012,21.9848772975832,-18.4122851134753));
#32530=CARTESIAN_POINT('Ctrl Pts',(-20.7753620094961,21.9089893790141,-18.4174956697838));
#32531=CARTESIAN_POINT('Ctrl Pts',(-20.8269260061065,21.8269709381329,-18.4233961208994));
#32532=CARTESIAN_POINT('Ctrl Pts',(-20.83198940777,21.8189950690965,-18.4239727974267));
#32533=CARTESIAN_POINT('Ctrl Pts',(-20.8395060741637,21.8072690877395,-18.4248249308773));
#32534=CARTESIAN_POINT('Ctrl Pts',(-20.8419322401638,21.803501593215,-18.4250993768899));
#32535=CARTESIAN_POINT('Ctrl Pts',(-20.8462070756401,21.7968936923288,-18.425581900644));
#32536=CARTESIAN_POINT('Ctrl Pts',(-20.848052386662,21.7940511127125,-18.4257898524937));
#32537=CARTESIAN_POINT('Ctrl Pts',(-20.8516463131601,21.7885339813305,-18.4261942059967));
#32538=CARTESIAN_POINT('Ctrl Pts',(-20.8533944301623,21.7858591080257,-18.4263905887921));
#32539=CARTESIAN_POINT('Ctrl Pts',(-20.8575807652294,21.7794741632461,-18.4268601714873));
#32540=CARTESIAN_POINT('Ctrl Pts',(-20.8600226724847,21.7757665282578,-18.4271335099537));
#32541=CARTESIAN_POINT('Ctrl Pts',(-20.8688049317978,21.7624919048084,-18.4281145331383));
#32542=CARTESIAN_POINT('Ctrl Pts',(-20.8751886617104,21.7529538430998,-18.4288238527858));
#32543=CARTESIAN_POINT('Ctrl Pts',(-20.9785398306536,21.600305177606,-18.4402480859513));
#32544=CARTESIAN_POINT('Ctrl Pts',(-21.0867994443325,21.4652148827186,-18.4514049328044));
#32545=CARTESIAN_POINT('Ctrl Pts',(-21.3646770035448,21.1704792752876,-18.4783165566837));
#32546=CARTESIAN_POINT('Ctrl Pts',(-21.5417916363208,21.0192179241965,-18.4942813455054));
#32547=CARTESIAN_POINT('Ctrl Pts',(-21.7948166535963,20.8465416646728,-18.5146317129483));
#32548=CARTESIAN_POINT('Ctrl Pts',(-21.8574449574504,20.806894767084,-18.5194875999644));
#32549=CARTESIAN_POINT('Ctrl Pts',(-21.9475497228463,20.7541158282959,-18.5261669380718));
#32550=CARTESIAN_POINT('Ctrl Pts',(-21.9739265294444,20.7391614166204,-18.5280864433305));
#32551=CARTESIAN_POINT('Ctrl Pts',(-22.00446069886,20.7224149376269,-18.5302642868526));
#32552=CARTESIAN_POINT('Ctrl Pts',(-22.0084143564803,20.7202573212886,-18.530545437944));
#32553=CARTESIAN_POINT('Ctrl Pts',(-22.0144225385172,20.7169948243676,-18.5309713966716));
#32554=CARTESIAN_POINT('Ctrl Pts',(-22.0164737399099,20.7158838855892,-18.5311165913318));
#32555=CARTESIAN_POINT('Ctrl Pts',(-22.0201692336278,20.7138875779177,-18.531377764323));
#32556=CARTESIAN_POINT('Ctrl Pts',(-22.0218130856495,20.713001413117,-18.5314937937483));
#32557=CARTESIAN_POINT('Ctrl Pts',(-22.025343970863,20.7111019490016,-18.5317427011315));
#32558=CARTESIAN_POINT('Ctrl Pts',(-22.027231238995,20.71008910468,-18.5318755495466));
#32559=CARTESIAN_POINT('Ctrl Pts',(-22.0323060928317,20.7073720846653,-18.5322322628288));
#32560=CARTESIAN_POINT('Ctrl Pts',(-22.035495550083,20.7056713825056,-18.5324559050817));
#32561=CARTESIAN_POINT('Ctrl Pts',(-22.0500737023155,20.6979294011274,-18.5334756543707));
#32562=CARTESIAN_POINT('Ctrl Pts',(-22.0614959299326,20.6919510158999,-18.5342678004516));
#32563=CARTESIAN_POINT('Ctrl Pts',(-22.2656934835936,20.5866303104901,-18.548313058811));
#32564=CARTESIAN_POINT('Ctrl Pts',(-22.4680098801037,20.5069104117566,-18.5604119558014));
#32565=CARTESIAN_POINT('Ctrl Pts',(-22.9408034806555,20.3737930195518,-18.5878595234725));
#32566=CARTESIAN_POINT('Ctrl Pts',(-23.2131382556604,20.3334760865714,-18.6031903870781));
#32567=CARTESIAN_POINT('Ctrl Pts',(-23.5043957681837,20.3277832947156,-18.6208446579915));
#32568=CARTESIAN_POINT('Ctrl Pts',(-23.5215195678297,20.3275851232959,-18.6218866651325));
#32569=CARTESIAN_POINT('Ctrl Pts',(-23.5443076332117,20.3275030379853,-18.6232790108695));
#32570=CARTESIAN_POINT('Ctrl Pts',(-23.5499714017471,20.3274975671743,-18.6236255309148));
#32571=CARTESIAN_POINT('Ctrl Pts',(-23.5592610076012,20.3275130825749,-18.6241946593744));
#32572=CARTESIAN_POINT('Ctrl Pts',(-23.5628868637297,20.3275252576247,-18.6244169908575));
#32573=CARTESIAN_POINT('Ctrl Pts',(-23.5699059049083,20.3275606721317,-18.6248477636452));
#32574=CARTESIAN_POINT('Ctrl Pts',(-23.5732990904062,20.3275831516987,-18.6250561808035));
#32575=CARTESIAN_POINT('Ctrl Pts',(-23.5811232230414,20.3276473436527,-18.625537152734));
#32576=CARTESIAN_POINT('Ctrl Pts',(-23.5855541248295,20.3276928356164,-18.6258098258307));
#32577=CARTESIAN_POINT('Ctrl Pts',(-23.5993438904945,20.3278628586427,-18.6266593531892));
#32578=CARTESIAN_POINT('Ctrl Pts',(-23.6087022524835,20.3280190215847,-18.627237199442));
#32579=CARTESIAN_POINT('Ctrl Pts',(-23.6881102002113,20.329690147829,-18.6321517456311));
#32580=CARTESIAN_POINT('Ctrl Pts',(-23.7580890866394,20.3334482903648,-18.6365585324857));
#32581=CARTESIAN_POINT('Ctrl Pts',(-23.836148137421,20.3401980083756,-18.641564836027));
#32582=CARTESIAN_POINT('Ctrl Pts',(-23.8444076800902,20.3409443372878,-18.6420956907095));
#32583=CARTESIAN_POINT('Ctrl Pts',(-23.8786744171778,20.3441740595482,-18.6443027704666));
#32584=CARTESIAN_POINT('Ctrl Pts',(-23.9046532727445,20.3469417196782,-18.6459872892983));
#32585=CARTESIAN_POINT('Ctrl Pts',(-24.2048989950582,20.3826254970169,-18.6655855722686));
#32586=CARTESIAN_POINT('Ctrl Pts',(-24.4738514568601,20.450358098373,-18.6845405247809));
#32587=CARTESIAN_POINT('Ctrl Pts',(-24.8105245870061,20.5829017473478,-18.708784564421));
#32588=CARTESIAN_POINT('Ctrl Pts',(-24.8889597853849,20.6174515754247,-18.7144600003672));
#32589=CARTESIAN_POINT('Ctrl Pts',(-24.9937431888341,20.6686885805699,-18.7219976110423));
#32590=CARTESIAN_POINT('Ctrl Pts',(-25.021359903857,20.6826892206582,-18.7239797914386));
#32591=CARTESIAN_POINT('Ctrl Pts',(-25.0635708684427,20.7048589552883,-18.7269977638478));
#32592=CARTESIAN_POINT('Ctrl Pts',(-25.0783097240559,20.7127468949328,-18.7280493186583));
#32593=CARTESIAN_POINT('Ctrl Pts',(-25.0963279723545,20.7225710122527,-18.7293314671674));
#32594=CARTESIAN_POINT('Ctrl Pts',(-25.0996658248035,20.724398591538,-18.7295688400058));
#32595=CARTESIAN_POINT('Ctrl Pts',(-25.1049112252408,20.7272827011938,-18.7299416340169));
#32596=CARTESIAN_POINT('Ctrl Pts',(-25.1068209377049,20.7283352552999,-18.7300773094332));
#32597=CARTESIAN_POINT('Ctrl Pts',(-25.1101975168179,20.7302007558514,-18.7303171094058));
#32598=CARTESIAN_POINT('Ctrl Pts',(-25.1116648093723,20.7310129047397,-18.7304212845952));
#32599=CARTESIAN_POINT('Ctrl Pts',(-25.114801510911,20.7327522742419,-18.7306439211502));
#32600=CARTESIAN_POINT('Ctrl Pts',(-25.1164707251204,20.7336798307436,-18.7307623600377));
#32601=CARTESIAN_POINT('Ctrl Pts',(-25.1212988698302,20.7363683752656,-18.7311048319742));
#32602=CARTESIAN_POINT('Ctrl Pts',(-25.1244556746874,20.7381332050536,-18.7313286172352));
#32603=CARTESIAN_POINT('Ctrl Pts',(-25.1385278664169,20.7460314655823,-18.7323256217192));
#32604=CARTESIAN_POINT('Ctrl Pts',(-25.149410618544,20.7522232695375,-18.7330951233033));
#32605=CARTESIAN_POINT('Ctrl Pts',(-25.1658708920401,20.7617158419241,-18.7342570966659));
#32606=CARTESIAN_POINT('Ctrl Pts',(-25.1714748417691,20.7649701798691,-18.7346523565235));
#32607=CARTESIAN_POINT('Ctrl Pts',(-25.1839891042055,20.7722880543678,-18.7355343485289));
#32608=CARTESIAN_POINT('Ctrl Pts',(-25.1908941732116,20.776360530794,-18.7360205523593));
#32609=CARTESIAN_POINT('Ctrl Pts',(-25.2044998312129,20.7844534620317,-18.7369778017514));
#32610=CARTESIAN_POINT('Ctrl Pts',(-25.211201129971,20.7884726023474,-18.7374489165066));
#32611=CARTESIAN_POINT('Ctrl Pts',(-25.3123063223608,20.8496120880592,-18.7445522958534));
#32612=CARTESIAN_POINT('Ctrl Pts',(-25.403740194443,20.9115254234033,-18.7509175933737));
#32613=CARTESIAN_POINT('Ctrl Pts',(-25.5461958201045,21.0190535360002,-18.761039318768));
#32614=CARTESIAN_POINT('Ctrl Pts',(-25.5992526125021,21.0618078255325,-18.7648589048497));
#32615=CARTESIAN_POINT('Ctrl Pts',(-25.7535175693735,21.1943992196435,-18.7762362958474));
#32616=CARTESIAN_POINT('Ctrl Pts',(-25.8504629604877,21.2889581587594,-18.7837603616064));
#32617=CARTESIAN_POINT('Ctrl Pts',(-26.0096059908036,21.4650395386185,-18.7972571773124));
#32618=CARTESIAN_POINT('Ctrl Pts',(-26.074395671517,21.5439545870268,-18.8031476437638));
#32619=CARTESIAN_POINT('Ctrl Pts',(-26.1611357459002,21.6604710416067,-18.8117369201242));
#32620=CARTESIAN_POINT('Ctrl Pts',(-26.1862414336318,21.6956508269345,-18.814316784412));
#32621=CARTESIAN_POINT('Ctrl Pts',(-26.2249120656496,21.7522107761879,-18.8184498485922));
#32622=CARTESIAN_POINT('Ctrl Pts',(-26.2389460385455,21.7732649271205,-18.8199852085452));
#32623=CARTESIAN_POINT('Ctrl Pts',(-26.2562553141048,21.7999073180454,-18.8219249601846));
#32624=CARTESIAN_POINT('Ctrl Pts',(-26.2597639182748,21.8053435167647,-18.822320591064));
#32625=CARTESIAN_POINT('Ctrl Pts',(-26.2653103972228,21.8139942458221,-18.8229499237613));
#32626=CARTESIAN_POINT('Ctrl Pts',(-26.2673590018506,21.8172019040248,-18.8231832252581));
#32627=CARTESIAN_POINT('Ctrl Pts',(-26.2712000184038,21.823239631013,-18.8236222695301));
#32628=CARTESIAN_POINT('Ctrl Pts',(-26.2729937107963,21.8260688825322,-18.8238279643233));
#32629=CARTESIAN_POINT('Ctrl Pts',(-26.2770068335159,21.8324207951588,-18.8242896812571));
#32630=CARTESIAN_POINT('Ctrl Pts',(-26.2792238521986,21.8359449661867,-18.8245457924001));
#32631=CARTESIAN_POINT('Ctrl Pts',(-26.2848275111551,21.8448909542795,-18.82519577833));
#32632=CARTESIAN_POINT('Ctrl Pts',(-26.2882048486781,21.8503185515071,-18.8255899963843));
#32633=CARTESIAN_POINT('Ctrl Pts',(-26.3065826923311,21.880049762623,-18.8277487520558));
#32634=CARTESIAN_POINT('Ctrl Pts',(-26.3212753830407,21.9045412821433,-18.8295245752832));
#32635=CARTESIAN_POINT('Ctrl Pts',(-26.5249390601308,22.2544934097971,-18.8548715028241));
#32636=CARTESIAN_POINT('Ctrl Pts',(-26.65576628624,22.610370572396,-18.8808216122646));
#32637=CARTESIAN_POINT('Ctrl Pts',(-26.7326788134364,23.0386288612668,-18.9098075378692));
#32638=CARTESIAN_POINT('Ctrl Pts',(-26.7415090870816,23.096955504035,-18.9136977982153));
#32639=CARTESIAN_POINT('Ctrl Pts',(-26.7551800657609,23.2077230855739,-18.9209397360323));
#32640=CARTESIAN_POINT('Ctrl Pts',(-26.7603463622836,23.2601054541113,-18.9243032076897));
#32641=CARTESIAN_POINT('Ctrl Pts',(-26.7646018312375,23.3176544112297,-18.927914464213));
#32642=CARTESIAN_POINT('Ctrl Pts',(-26.764964040301,23.3227152327999,-18.9282313250719));
#32643=CARTESIAN_POINT('Ctrl Pts',(-26.7654819660451,23.3301999333398,-18.9286988741158));
#32644=CARTESIAN_POINT('Ctrl Pts',(-26.7656468943645,23.332623135334,-18.9288500788735));
#32645=CARTESIAN_POINT('Ctrl Pts',(-26.765922868151,23.3367466695968,-18.9291070968865));
#32646=CARTESIAN_POINT('Ctrl Pts',(-26.7660353045173,23.3384469038467,-18.9292129891401));
#32647=CARTESIAN_POINT('Ctrl Pts',(-26.7662626964322,23.3419273885443,-18.9294295873037));
#32648=CARTESIAN_POINT('Ctrl Pts',(-26.7663775220232,23.343707641689,-18.9295402855908));
#32649=CARTESIAN_POINT('Ctrl Pts',(-26.7666492496946,23.3479756705539,-18.9298054611776));
#32650=CARTESIAN_POINT('Ctrl Pts',(-26.7668047440432,23.3504635393855,-18.9299598586127));
#32651=CARTESIAN_POINT('Ctrl Pts',(-26.7672696396885,23.3580429867806,-18.9304297119781));
#32652=CARTESIAN_POINT('Ctrl Pts',(-26.7675698411566,23.3631351531289,-18.9307446518818));
#32653=CARTESIAN_POINT('Ctrl Pts',(-26.7706837640678,23.4181792618025,-18.934141378813));
#32654=CARTESIAN_POINT('Ctrl Pts',(-26.7723461947943,23.4681929285441,-18.9371597307708));
#32655=CARTESIAN_POINT('Ctrl Pts',(-26.7729447253812,23.5284229979129,-18.9407345898242));
#32656=CARTESIAN_POINT('Ctrl Pts',(-26.7729976582524,23.5386181950847,-18.9413376384116));
#32657=CARTESIAN_POINT('Ctrl Pts',(-26.7730372952479,23.6273916831091,-18.9465718943153));
#32658=CARTESIAN_POINT('Ctrl Pts',(-26.7701984882302,23.7059499859438,-18.9510901250681));
#32659=CARTESIAN_POINT('Ctrl Pts',(-26.738507148839,24.1411189798893,-18.9758586346407));
#32660=CARTESIAN_POINT('Ctrl Pts',(-26.6533123248868,24.491058250259,-18.9951350607033));
#32661=CARTESIAN_POINT('Ctrl Pts',(-26.5043364157131,24.8386324304217,-19.018003598287));
#32662=CARTESIAN_POINT('Ctrl Pts',(-26.4961156515518,24.8573197857052,-19.0192441377773));
#32663=CARTESIAN_POINT('Ctrl Pts',(-26.4851442788581,24.8816304432354,-19.0208728439227));
#32664=CARTESIAN_POINT('Ctrl Pts',(-26.4825539338123,24.887325901848,-19.0212554876822));
#32665=CARTESIAN_POINT('Ctrl Pts',(-26.4785377007967,24.8960886927518,-19.0218458757334));
#32666=CARTESIAN_POINT('Ctrl Pts',(-26.4771235320184,24.8991614060509,-19.0220532150047));
#32667=CARTESIAN_POINT('Ctrl Pts',(-26.4743021609076,24.9052663704381,-19.0224657964235));
#32668=CARTESIAN_POINT('Ctrl Pts',(-26.4728950728785,24.9082986699445,-19.0226710344182));
#32669=CARTESIAN_POINT('Ctrl Pts',(-26.4697718026634,24.9150020365453,-19.0231254363995));
#32670=CARTESIAN_POINT('Ctrl Pts',(-26.4680534110744,24.9186720626133,-19.0233746767447));
#32671=CARTESIAN_POINT('Ctrl Pts',(-26.4630945008023,24.9292111644222,-19.0240917412002));
#32672=CARTESIAN_POINT('Ctrl Pts',(-26.4598366318303,24.9360720042177,-19.0245601675125));
#32673=CARTESIAN_POINT('Ctrl Pts',(-26.4381922633688,24.9812407314923,-19.0276548966073));
#32674=CARTESIAN_POINT('Ctrl Pts',(-26.419074652922,25.0191917678929,-19.0303066236142));
#32675=CARTESIAN_POINT('Ctrl Pts',(-26.3606375898138,25.1297028239749,-19.0381859472661));
#32676=CARTESIAN_POINT('Ctrl Pts',(-26.3192775248967,25.201138970678,-19.0434844162707));
#32677=CARTESIAN_POINT('Ctrl Pts',(-26.1157899912737,25.523399291582,-19.0683554509675));
#32678=CARTESIAN_POINT('Ctrl Pts',(-25.9220696746796,25.7524630989853,-19.0890227882896));
#32679=CARTESIAN_POINT('Ctrl Pts',(-25.6330270212063,26.0111781413648,-19.1146742047232));
#32680=CARTESIAN_POINT('Ctrl Pts',(-25.5639785225902,26.0679926942967,-19.1204752568961));
#32681=CARTESIAN_POINT('Ctrl Pts',(-25.4875407475089,26.125727814493,-19.1264803784946));
#32682=CARTESIAN_POINT('Ctrl Pts',(-25.4824197283844,26.12957191656,-19.1268807615697));
#32683=CARTESIAN_POINT('Ctrl Pts',(-25.4753025829964,26.1348813238737,-19.1274344923704));
#32684=CARTESIAN_POINT('Ctrl Pts',(-25.4733162179885,26.1363595967515,-19.1275887438654));
#32685=CARTESIAN_POINT('Ctrl Pts',(-25.469899363085,26.1388963410757,-19.1278535752755));
#32686=CARTESIAN_POINT('Ctrl Pts',(-25.4684697005586,26.1399559166839,-19.1279642330125));
#32687=CARTESIAN_POINT('Ctrl Pts',(-25.4655149393362,26.1421420099164,-19.1281926210819));
#32688=CARTESIAN_POINT('Ctrl Pts',(-25.4639897269814,26.1432683636616,-19.1283103394235));
#32689=CARTESIAN_POINT('Ctrl Pts',(-25.4604069392783,26.1459093328407,-19.1285864612054));
#32690=CARTESIAN_POINT('Ctrl Pts',(-25.458348549777,26.1474228526466,-19.1287447873349));
#32691=CARTESIAN_POINT('Ctrl Pts',(-25.4516596136515,26.1523289376635,-19.1292582796233));
#32692=CARTESIAN_POINT('Ctrl Pts',(-25.4470217685376,26.1557116039476,-19.1296127556672));
#32693=CARTESIAN_POINT('Ctrl Pts',(-25.3166527291841,26.2502651899831,-19.1395341189983));
#32694=CARTESIAN_POINT('Ctrl Pts',(-25.1844832161355,26.3322559317665,-19.1484790605671));
#32695=CARTESIAN_POINT('Ctrl Pts',(-24.7447150827609,26.5628591746677,-19.1765241230685));
#32696=CARTESIAN_POINT('Ctrl Pts',(-24.4193256523109,26.6723102604059,-19.1950478732565));
#32697=CARTESIAN_POINT('Ctrl Pts',(-24.0628041742597,26.7320476646317,-19.2169102087032));
#32698=CARTESIAN_POINT('Ctrl Pts',(-24.0427572216129,26.7352122732593,-19.2181434826066));
#32699=CARTESIAN_POINT('Ctrl Pts',(-24.0165071496756,26.7391023495238,-19.2197639699858));
#32700=CARTESIAN_POINT('Ctrl Pts',(-24.0103296223558,26.7399994807864,-19.2201457297175));
#32701=CARTESIAN_POINT('Ctrl Pts',(-24.000803646443,26.7413546418142,-19.2207350532318));
#32702=CARTESIAN_POINT('Ctrl Pts',(-23.9974569947268,26.741825365317,-19.2209422143555));
#32703=CARTESIAN_POINT('Ctrl Pts',(-23.9907984052143,26.7427512508724,-19.2213546306447));
#32704=CARTESIAN_POINT('Ctrl Pts',(-23.9874864871222,26.7432065255245,-19.2215598819665));
#32705=CARTESIAN_POINT('Ctrl Pts',(-23.9802345575883,26.7441919213293,-19.2220095737955));
#32706=CARTESIAN_POINT('Ctrl Pts',(-23.9762942657422,26.7447199063715,-19.2222540816298));
#32707=CARTESIAN_POINT('Ctrl Pts',(-23.9650721674279,26.7462024950677,-19.2229509398948));
#32708=CARTESIAN_POINT('Ctrl Pts',(-23.9577880958527,26.7471394957723,-19.2234038468337));
#32709=CARTESIAN_POINT('Ctrl Pts',(-23.9414485928975,26.7491846086234,-19.2244211434862));
#32710=CARTESIAN_POINT('Ctrl Pts',(-23.9323915583628,26.7502791804348,-19.2249859584167));
#32711=CARTESIAN_POINT('Ctrl Pts',(-23.7357485100187,26.7731973961969,-19.2372694933105));
#32712=CARTESIAN_POINT('Ctrl Pts',(-23.5466435914315,26.7785255136717,-19.2495201031416));
#32713=CARTESIAN_POINT('Ctrl Pts',(-23.0793767528534,26.7506285470333,-19.2807733954771));
#32714=CARTESIAN_POINT('Ctrl Pts',(-22.8039219727572,26.6978104959097,-19.3001285623604));
#32715=CARTESIAN_POINT('Ctrl Pts',(-22.5027167431305,26.598239557912,-19.3205357950218));
#32716=CARTESIAN_POINT('Ctrl Pts',(-22.4669157934068,26.5856994455135,-19.3229464002846));
#32717=CARTESIAN_POINT('Ctrl Pts',(-22.4264223849635,26.570707942943,-19.3256491606233));
#32718=CARTESIAN_POINT('Ctrl Pts',(-22.4215065015531,26.5688743182733,-19.3259768716167));
#32719=CARTESIAN_POINT('Ctrl Pts',(-22.4143148143236,26.5661717943083,-19.3264556822973));
#32720=CARTESIAN_POINT('Ctrl Pts',(-22.4120355151096,26.5653123187637,-19.3266073438389));
#32721=CARTESIAN_POINT('Ctrl Pts',(-22.4079950191913,26.5637834984208,-19.3268760297899));
#32722=CARTESIAN_POINT('Ctrl Pts',(-22.4062334341881,26.5631151931682,-19.3269931169525));
#32723=CARTESIAN_POINT('Ctrl Pts',(-22.4025487295212,26.561713602506,-19.3272379114874));
#32724=CARTESIAN_POINT('Ctrl Pts',(-22.4006257302273,26.5609800211797,-19.3273656003782));
#32725=CARTESIAN_POINT('Ctrl Pts',(-22.3955894630251,26.5590532689303,-19.3276998429006));
#32726=CARTESIAN_POINT('Ctrl Pts',(-22.3924773313694,26.557857104156,-19.3279062155926));
#32727=CARTESIAN_POINT('Ctrl Pts',(-22.3788173781799,26.5525824824962,-19.3288113130218));
#32728=CARTESIAN_POINT('Ctrl Pts',(-22.3682890413697,26.5484532869622,-19.3295070095386));
#32729=CARTESIAN_POINT('Ctrl Pts',(-22.2912232514053,26.5177591816892,-19.3345869440783));
#32730=CARTESIAN_POINT('Ctrl Pts',(-22.2255606086061,26.4890351958121,-19.3388470206358));
#32731=CARTESIAN_POINT('Ctrl Pts',(-22.1320704356073,26.4443669586381,-19.3448884612601));
#32732=CARTESIAN_POINT('Ctrl Pts',(-22.103444381051,26.4301630688019,-19.3467349361993));
#32733=CARTESIAN_POINT('Ctrl Pts',(-22.0750360113656,26.4155367725069,-19.3485684984428));
#32734=CARTESIAN_POINT('',(-26.7730018214075,23.5481128698841,-19.1857734492732));
#32735=CARTESIAN_POINT('Ctrl Pts',(-22.075036015346,26.4155367745563,-19.592915740792));
#32736=CARTESIAN_POINT('Ctrl Pts',(-22.1638817756157,26.4612797870632,-19.5867644769599));
#32737=CARTESIAN_POINT('Ctrl Pts',(-22.2548303270937,26.5028728174781,-19.5806132131277));
#32738=CARTESIAN_POINT('Ctrl Pts',(-22.3474545181231,26.5401345529535,-19.5744619492956));
#32739=CARTESIAN_POINT('Ctrl Pts',(-22.4401819008943,26.5774378013786,-19.5683038323982));
#32740=CARTESIAN_POINT('Ctrl Pts',(-22.5345882459535,26.6103999605182,-19.5621457155008));
#32741=CARTESIAN_POINT('Ctrl Pts',(-22.6302284943965,26.6388886924121,-19.5559875986034));
#32742=CARTESIAN_POINT('Ctrl Pts',(-22.7259291705768,26.6673954241507,-19.5498255908643));
#32743=CARTESIAN_POINT('Ctrl Pts',(-22.8228648810819,26.6914229971941,-19.5436635831252));
#32744=CARTESIAN_POINT('Ctrl Pts',(-22.9205795626509,26.7108900488031,-19.537501575386));
#32745=CARTESIAN_POINT('Ctrl Pts',(-23.0184488317674,26.7303878978696,-19.5313298191664));
#32746=CARTESIAN_POINT('Ctrl Pts',(-23.1170991033048,26.7453107579507,-19.5251580629468));
#32747=CARTESIAN_POINT('Ctrl Pts',(-23.2160684532901,26.7556290406618,-19.5189863067272));
#32748=CARTESIAN_POINT('Ctrl Pts',(-23.2611536717233,26.7603295063105,-19.5161747799533));
#32749=CARTESIAN_POINT('Ctrl Pts',(-23.3063050959804,26.7640751313075,-19.5133632531795));
#32750=CARTESIAN_POINT('Ctrl Pts',(-23.3514791794028,26.7668667014259,-19.5105517264056));
#32751=CARTESIAN_POINT('Ctrl Pts',(-23.4506489865071,26.7729949822716,-19.5043796350932));
#32752=CARTESIAN_POINT('Ctrl Pts',(-23.550277124991,26.7745435777351,-19.4982075437809));
#32753=CARTESIAN_POINT('Ctrl Pts',(-23.6499048733714,26.7714614620957,-19.4920354524686));
#32754=CARTESIAN_POINT('Ctrl Pts',(-23.749397636002,26.7683835224183,-19.4858717237298));
#32755=CARTESIAN_POINT('Ctrl Pts',(-23.8488895792128,26.7606873555042,-19.479707994991));
#32756=CARTESIAN_POINT('Ctrl Pts',(-23.9479181499618,26.7483737955846,-19.4735442662523));
#32757=CARTESIAN_POINT('Ctrl Pts',(-24.0468418092345,26.736073280726,-19.4673870674056));
#32758=CARTESIAN_POINT('Ctrl Pts',(-24.1453026432962,26.7191651513008,-19.4612298685589));
#32759=CARTESIAN_POINT('Ctrl Pts',(-24.2428403636803,26.6977022385974,-19.4550726697122));
#32760=CARTESIAN_POINT('Ctrl Pts',(-24.3403067899057,26.6762550139816,-19.4489199714045));
#32761=CARTESIAN_POINT('Ctrl Pts',(-24.4368510209793,26.650259718311,-19.4427672730968));
#32762=CARTESIAN_POINT('Ctrl Pts',(-24.5320210574339,26.6198205997401,-19.4366145747891));
#32763=CARTESIAN_POINT('Ctrl Pts',(-24.6271550052752,26.5893930237263,-19.4304642095933));
#32764=CARTESIAN_POINT('Ctrl Pts',(-24.7209153806172,26.554525105284,-19.4243138443976));
#32765=CARTESIAN_POINT('Ctrl Pts',(-24.8128643577964,26.5153712374271,-19.4181634792018));
#32766=CARTESIAN_POINT('Ctrl Pts',(-24.9048030668498,26.4762217419607,-19.4120138008296));
#32767=CARTESIAN_POINT('Ctrl Pts',(-24.99493038023,26.4327874188326,-19.4058641224574));
#32768=CARTESIAN_POINT('Ctrl Pts',(-25.0828284499124,26.3852708063086,-19.3997144440852));
#32769=CARTESIAN_POINT('Ctrl Pts',(-25.1707402189784,26.3377467880668,-19.3935638072528));
#32770=CARTESIAN_POINT('Ctrl Pts',(-25.2564216720679,26.2861394232798,-19.3874131704204));
#32771=CARTESIAN_POINT('Ctrl Pts',(-25.3394804587469,26.2306967089817,-19.3812625335879));
#32772=CARTESIAN_POINT('Ctrl Pts',(-25.4226281008802,26.1751946826258,-19.3751053168661));
#32773=CARTESIAN_POINT('Ctrl Pts',(-25.5031471118834,26.1158493550813,-19.3689481001443));
#32774=CARTESIAN_POINT('Ctrl Pts',(-25.5806751023678,26.0529514242898,-19.3627908834225));
#32775=CARTESIAN_POINT('Ctrl Pts',(-25.6582463454004,25.9900184030004,-19.3566302316147));
#32776=CARTESIAN_POINT('Ctrl Pts',(-25.7328229205091,25.9235291204702,-19.3504695798069));
#32777=CARTESIAN_POINT('Ctrl Pts',(-25.8040780239711,25.8538124316888,-19.3443089279991));
#32778=CARTESIAN_POINT('Ctrl Pts',(-25.8754523625599,25.7839790820953,-19.3381379672301));
#32779=CARTESIAN_POINT('Ctrl Pts',(-25.9434938313503,25.7109078567522,-19.331967006461));
#32780=CARTESIAN_POINT('Ctrl Pts',(-26.0079146747089,25.6349621885271,-19.325796045692));
#32781=CARTESIAN_POINT('Ctrl Pts',(-26.0570883140048,25.5769914340214,-19.3210856354715));
#32782=CARTESIAN_POINT('Ctrl Pts',(-26.1041531826861,25.5173465854334,-19.3163752252511));
#32783=CARTESIAN_POINT('Ctrl Pts',(-26.1489985783231,25.4562002087385,-19.3116648150306));
#32784=CARTESIAN_POINT('Ctrl Pts',(-26.2081317902181,25.37557249661,-19.3054536604244));
#32785=CARTESIAN_POINT('Ctrl Pts',(-26.2636129571008,25.292048867266,-19.2992425058183));
#32786=CARTESIAN_POINT('Ctrl Pts',(-26.3151478242801,25.2059915158147,-19.2930313512121));
#32787=CARTESIAN_POINT('Ctrl Pts',(-26.3666114707859,25.1200530947665,-19.2868287803597));
#32788=CARTESIAN_POINT('Ctrl Pts',(-26.414139439793,25.0315882738076,-19.2806262095074));
#32789=CARTESIAN_POINT('Ctrl Pts',(-26.4574788902681,24.9409906315941,-19.274423638655));
#32790=CARTESIAN_POINT('Ctrl Pts',(-26.5007695487846,24.8504949850534,-19.2682280507149));
#32791=CARTESIAN_POINT('Ctrl Pts',(-26.5398808802617,24.7578716736682,-19.2620324627749));
#32792=CARTESIAN_POINT('Ctrl Pts',(-26.5746048697898,24.6635406783821,-19.2558368748348));
#32793=CARTESIAN_POINT('Ctrl Pts',(-26.6092963985878,24.5692978657333,-19.2496470786631));
#32794=CARTESIAN_POINT('Ctrl Pts',(-26.6396085982497,24.4733509444553,-19.2434572824915));
#32795=CARTESIAN_POINT('Ctrl Pts',(-26.6653811061292,24.3761408578247,-19.2372674863199));
#32796=CARTESIAN_POINT('Ctrl Pts',(-26.691139177631,24.278985223075,-19.2310811573404));
#32797=CARTESIAN_POINT('Ctrl Pts',(-26.7123625051649,24.1805682420417,-19.2248948283609));
#32798=CARTESIAN_POINT('Ctrl Pts',(-26.7289404592313,24.0813463292759,-19.2187084993813));
#32799=CARTESIAN_POINT('Ctrl Pts',(-26.745516241683,23.9821374139982,-19.2125229807746));
#32800=CARTESIAN_POINT('Ctrl Pts',(-26.7574477822821,23.8821241963588,-19.2063374621679));
#32801=CARTESIAN_POINT('Ctrl Pts',(-26.7646756306367,23.7817729486884,-19.2001519435611));
#32802=CARTESIAN_POINT('Ctrl Pts',(-26.7702761082946,23.7040160709902,-19.1953591121318));
#32803=CARTESIAN_POINT('Ctrl Pts',(-26.773053570087,23.6260565053534,-19.1905662807025));
#32804=CARTESIAN_POINT('Ctrl Pts',(-26.7730018214075,23.5481128698841,-19.1857734492732));
#32805=CARTESIAN_POINT('Ctrl Pts',(-26.7730017222135,23.5479683454044,-19.1879840164276));
#32806=CARTESIAN_POINT('Ctrl Pts',(-26.7727851743233,23.2424418036611,-19.1680091024078));
#32807=CARTESIAN_POINT('Ctrl Pts',(-26.7291278268916,22.9385397708267,-19.1468119365999));
#32808=CARTESIAN_POINT('Ctrl Pts',(-26.6283095396878,22.5939304488475,-19.1231910839668));
#32809=CARTESIAN_POINT('Ctrl Pts',(-26.6119884302315,22.5428991258433,-19.1197103222852));
#32810=CARTESIAN_POINT('Ctrl Pts',(-26.5855073949,22.4667030152096,-19.1145627778049));
#32811=CARTESIAN_POINT('Ctrl Pts',(-26.576290339709,22.4412228014047,-19.1128499526712));
#32812=CARTESIAN_POINT('Ctrl Pts',(-26.5652069471654,22.4117505691125,-19.1108812278628));
#32813=CARTESIAN_POINT('Ctrl Pts',(-26.5636528152118,22.4076434217999,-19.1106071561069));
#32814=CARTESIAN_POINT('Ctrl Pts',(-26.5612754264844,22.4013992190108,-19.1101909225071));
#32815=CARTESIAN_POINT('Ctrl Pts',(-26.5604582865436,22.3992598642265,-19.1100483943854));
#32816=CARTESIAN_POINT('Ctrl Pts',(-26.5589716268404,22.3953800511084,-19.1097900602408));
#32817=CARTESIAN_POINT('Ctrl Pts',(-26.5583028790647,22.3936393086812,-19.1096742081957));
#32818=CARTESIAN_POINT('Ctrl Pts',(-26.5569534186101,22.3901357660666,-19.1094411446805));
#32819=CARTESIAN_POINT('Ctrl Pts',(-26.5562726691571,22.3883729912583,-19.1093239361097));
#32820=CARTESIAN_POINT('Ctrl Pts',(-26.5543204380999,22.383330963498,-19.1089888420098));
#32821=CARTESIAN_POINT('Ctrl Pts',(-26.5530451331687,22.3800531788366,-19.1087711876993));
#32822=CARTESIAN_POINT('Ctrl Pts',(-26.5475218182632,22.3659256561478,-19.1078338633722));
#32823=CARTESIAN_POINT('Ctrl Pts',(-26.5432202822737,22.3550967350997,-19.1071173882909));
#32824=CARTESIAN_POINT('Ctrl Pts',(-26.4684372615227,22.1697698191272,-19.0948859760059));
#32825=CARTESIAN_POINT('Ctrl Pts',(-26.382850748013,22.0017226862924,-19.0842479495856));
#32826=CARTESIAN_POINT('Ctrl Pts',(-26.1946319991938,21.7005999602954,-19.0643573407785));
#32827=CARTESIAN_POINT('Ctrl Pts',(-26.0953436979259,21.5661995676183,-19.0551114814917));
#32828=CARTESIAN_POINT('Ctrl Pts',(-25.9360271155736,21.38229382275,-19.0411969509695));
#32829=CARTESIAN_POINT('Ctrl Pts',(-25.8839178786734,21.3262987954141,-19.0367690107676));
#32830=CARTESIAN_POINT('Ctrl Pts',(-25.7786063710529,21.2209144114224,-19.027989646342));
#32831=CARTESIAN_POINT('Ctrl Pts',(-25.7256302583036,21.1713646818381,-19.023648701961));
#32832=CARTESIAN_POINT('Ctrl Pts',(-25.6645590027993,21.1179902947171,-19.0187056806998));
#32833=CARTESIAN_POINT('Ctrl Pts',(-25.6580644561203,21.1123599310708,-19.0181807777443));
#32834=CARTESIAN_POINT('Ctrl Pts',(-25.6489488222144,21.1045209049677,-19.0174450562022));
#32835=CARTESIAN_POINT('Ctrl Pts',(-25.6463465769597,21.1022903050509,-19.0172351452867));
#32836=CARTESIAN_POINT('Ctrl Pts',(-25.6413477613603,21.0980192209926,-19.0168321338162));
#32837=CARTESIAN_POINT('Ctrl Pts',(-25.6389517491361,21.095978087262,-19.0166390603576));
#32838=CARTESIAN_POINT('Ctrl Pts',(-25.6339417453161,21.0917227761092,-19.0162355473379));
#32839=CARTESIAN_POINT('Ctrl Pts',(-25.6313272070536,21.0895092509987,-19.0160250813059));
#32840=CARTESIAN_POINT('Ctrl Pts',(-25.6255612101237,21.0846433943147,-19.0155611731351));
#32841=CARTESIAN_POINT('Ctrl Pts',(-25.6224081890818,21.0819929301925,-19.0153076548332));
#32842=CARTESIAN_POINT('Ctrl Pts',(-25.6114011369336,21.0727762369637,-19.0144231858524));
#32843=CARTESIAN_POINT('Ctrl Pts',(-25.603520969599,21.0662414443892,-19.0137909530803));
#32844=CARTESIAN_POINT('Ctrl Pts',(-25.523549154059,21.0005637074516,-19.0073842716041));
#32845=CARTESIAN_POINT('Ctrl Pts',(-25.4489607177624,20.944543995985,-19.0014847619186));
#32846=CARTESIAN_POINT('Ctrl Pts',(-25.2887092551718,20.8347241236295,-18.9889437212693));
#32847=CARTESIAN_POINT('Ctrl Pts',(-25.2027307802655,20.7815635108702,-18.9822879953149));
#32848=CARTESIAN_POINT('Ctrl Pts',(-25.0542620623923,20.6991466872039,-18.9709478547943));
#32849=CARTESIAN_POINT('Ctrl Pts',(-24.9930684421427,20.667696213721,-18.9663156439852));
#32850=CARTESIAN_POINT('Ctrl Pts',(-24.8100347282932,20.5809152700826,-18.952625691578));
#32851=CARTESIAN_POINT('Ctrl Pts',(-24.6856986754023,20.5311833786956,-18.9435300632271));
#32852=CARTESIAN_POINT('Ctrl Pts',(-24.5083866875914,20.4727706395849,-18.9310850111468));
#32853=CARTESIAN_POINT('Ctrl Pts',(-24.457741506682,20.4574576538197,-18.9275889483037));
#32854=CARTESIAN_POINT('Ctrl Pts',(-24.3666222173832,20.4323381887796,-18.9214282686706));
#32855=CARTESIAN_POINT('Ctrl Pts',(-24.3262917772876,20.4220561227769,-18.9187459978098));
#32856=CARTESIAN_POINT('Ctrl Pts',(-24.2655166518835,20.4078095966196,-18.9147817170289));
#32857=CARTESIAN_POINT('Ctrl Pts',(-24.2452157306226,20.4032576844156,-18.9134704075289));
#32858=CARTESIAN_POINT('Ctrl Pts',(-24.2208811617263,20.3980483099226,-18.9119151055985));
#32859=CARTESIAN_POINT('Ctrl Pts',(-24.2168891572155,20.3972016559351,-18.9116604949295));
#32860=CARTESIAN_POINT('Ctrl Pts',(-24.2107192964807,20.3959053472258,-18.9112678124196));
#32861=CARTESIAN_POINT('Ctrl Pts',(-24.2085425832429,20.3954503642587,-18.9111294347809));
#32862=CARTESIAN_POINT('Ctrl Pts',(-24.204721417179,20.3946557798971,-18.9108867989433));
#32863=CARTESIAN_POINT('Ctrl Pts',(-24.2030771764796,20.3943152120986,-18.9107824851344));
#32864=CARTESIAN_POINT('Ctrl Pts',(-24.1995920177915,20.3935961794033,-18.9105615747626));
#32865=CARTESIAN_POINT('Ctrl Pts',(-24.1977510402101,20.393218040882,-18.9104449974503));
#32866=CARTESIAN_POINT('Ctrl Pts',(-24.1925136743651,20.3921470548996,-18.9101136728131));
#32867=CARTESIAN_POINT('Ctrl Pts',(-24.1891164843744,20.3914580736486,-18.9098991484444));
#32868=CARTESIAN_POINT('Ctrl Pts',(-24.1747105180798,20.3885606023934,-18.908991063629));
#32869=CARTESIAN_POINT('Ctrl Pts',(-24.1636911791029,20.3864041365891,-18.9083004574845));
#32870=CARTESIAN_POINT('Ctrl Pts',(-23.9701402187951,20.3495757717686,-18.8962367605639));
#32871=CARTESIAN_POINT('Ctrl Pts',(-23.7849272988383,20.3306893285851,-18.8857207502765));
#32872=CARTESIAN_POINT('Ctrl Pts',(-23.4313002381038,20.3253294054016,-18.8659029823924));
#32873=CARTESIAN_POINT('Ctrl Pts',(-23.2635699743342,20.3358956868316,-18.8566088604368));
#32874=CARTESIAN_POINT('Ctrl Pts',(-22.9940877148605,20.3741397411742,-18.8410536659842));
#32875=CARTESIAN_POINT('Ctrl Pts',(-22.8915298939915,20.3938157409492,-18.834987326594));
#32876=CARTESIAN_POINT('Ctrl Pts',(-22.7595035902304,20.4258604553327,-18.8268872276437));
#32877=CARTESIAN_POINT('Ctrl Pts',(-22.7290049573259,20.4337381242611,-18.8249957437281));
#32878=CARTESIAN_POINT('Ctrl Pts',(-22.6795406433711,20.4472910387426,-18.8218924719085));
#32879=CARTESIAN_POINT('Ctrl Pts',(-22.6605027274858,20.4526963210785,-18.8206894285754));
#32880=CARTESIAN_POINT('Ctrl Pts',(-22.6358385380682,20.4599451634573,-18.8191192012695));
#32881=CARTESIAN_POINT('Ctrl Pts',(-22.6301655858851,20.4616294414917,-18.8187572332951));
#32882=CARTESIAN_POINT('Ctrl Pts',(-22.6209990340417,20.4643784515717,-18.8181710408125));
#32883=CARTESIAN_POINT('Ctrl Pts',(-22.6175025309151,20.465433519638,-18.8179471333759));
#32884=CARTESIAN_POINT('Ctrl Pts',(-22.6107896615104,20.4674715810982,-18.8175166602941));
#32885=CARTESIAN_POINT('Ctrl Pts',(-22.6075730240163,20.4684536707237,-18.8173101245567));
#32886=CARTESIAN_POINT('Ctrl Pts',(-22.6002545045834,20.4707006590298,-18.8168396090541));
#32887=CARTESIAN_POINT('Ctrl Pts',(-22.5961536068795,20.471968719352,-18.816575525666));
#32888=CARTESIAN_POINT('Ctrl Pts',(-22.5836973058663,20.4758476807298,-18.8157720618658));
#32889=CARTESIAN_POINT('Ctrl Pts',(-22.5753500472922,20.4784844194027,-18.815231831985));
#32890=CARTESIAN_POINT('Ctrl Pts',(-22.5161985416387,20.497434634842,-18.8113905867852));
#32891=CARTESIAN_POINT('Ctrl Pts',(-22.4657981816182,20.5149728120127,-18.8080492954933));
#32892=CARTESIAN_POINT('Ctrl Pts',(-22.4054743031966,20.5376583909354,-18.8039635722731));
#32893=CARTESIAN_POINT('Ctrl Pts',(-22.3951102168828,20.5416171471634,-18.8032584970778));
#32894=CARTESIAN_POINT('Ctrl Pts',(-22.1933274174503,20.619888178015,-18.7894699363532));
#32895=CARTESIAN_POINT('Ctrl Pts',(-22.0094531657702,20.7122614412642,-18.7757827427425));
#32896=CARTESIAN_POINT('Ctrl Pts',(-21.7020842150694,20.9053950298511,-18.7512401506563));
#32897=CARTESIAN_POINT('Ctrl Pts',(-21.574864167231,20.999009284987,-18.7405085025313));
#32898=CARTESIAN_POINT('Ctrl Pts',(-21.4101263058538,21.1399690771474,-18.7262078865154));
#32899=CARTESIAN_POINT('Ctrl Pts',(-21.3663067844025,21.1796010350458,-18.72236179553));
#32900=CARTESIAN_POINT('Ctrl Pts',(-21.3037535050426,21.2393840287388,-18.7168388324749));
#32901=CARTESIAN_POINT('Ctrl Pts',(-21.2841506326168,21.2586039065244,-18.7151031527016));
#32902=CARTESIAN_POINT('Ctrl Pts',(-21.261688341662,21.281197458358,-18.7131111243461));
#32903=CARTESIAN_POINT('Ctrl Pts',(-21.2585881168428,21.284328616823,-18.7128361152916));
#32904=CARTESIAN_POINT('Ctrl Pts',(-21.2538841534632,21.2890990444458,-18.7124187506081));
#32905=CARTESIAN_POINT('Ctrl Pts',(-21.252275742674,21.2907336672813,-18.7122760256658));
#32906=CARTESIAN_POINT('Ctrl Pts',(-21.2493624761166,21.2937007390973,-18.7120174841272));
#32907=CARTESIAN_POINT('Ctrl Pts',(-21.2480570363215,21.295032599699,-18.7119016211253));
#32908=CARTESIAN_POINT('Ctrl Pts',(-21.2452338089533,21.2979179723267,-18.7116510267126));
#32909=CARTESIAN_POINT('Ctrl Pts',(-21.2437164396839,21.2994718813803,-18.7115163285433));
#32910=CARTESIAN_POINT('Ctrl Pts',(-21.2395884277564,21.303707858168,-18.7111498394251));
#32911=CARTESIAN_POINT('Ctrl Pts',(-21.2369808744193,21.3063929524509,-18.7109182923639));
#32912=CARTESIAN_POINT('Ctrl Pts',(-21.2245467215858,21.3192415711978,-18.7098139017879));
#32913=CARTESIAN_POINT('Ctrl Pts',(-21.2147821935364,21.329465342895,-18.708945861074));
#32914=CARTESIAN_POINT('Ctrl Pts',(-21.0367734704654,21.5183187274303,-18.6930997606971));
#32915=CARTESIAN_POINT('Ctrl Pts',(-20.8893759641594,21.7155562691804,-18.6795839602382));
#32916=CARTESIAN_POINT('Ctrl Pts',(-20.6901999939081,22.0573514762352,-18.6574639116931));
#32917=CARTESIAN_POINT('Ctrl Pts',(-20.6237753719986,22.1921727410893,-18.6490265385683));
#32918=CARTESIAN_POINT('Ctrl Pts',(-20.540084517025,22.3969678528042,-18.6361706441773));
#32919=CARTESIAN_POINT('Ctrl Pts',(-20.5153657563358,22.4636807664651,-18.6319789214494));
#32920=CARTESIAN_POINT('Ctrl Pts',(-20.485255674619,22.554013371,-18.6262700132007));
#32921=CARTESIAN_POINT('Ctrl Pts',(-20.4778926881231,22.5769575389117,-18.6248172296217));
#32922=CARTESIAN_POINT('Ctrl Pts',(-20.4676181586077,22.6102533619206,-18.622704168575));
#32923=CARTESIAN_POINT('Ctrl Pts',(-20.4644999259151,22.6205407651366,-18.6220506356219));
#32924=CARTESIAN_POINT('Ctrl Pts',(-20.4590382420843,22.6388896755676,-18.6208837158024));
#32925=CARTESIAN_POINT('Ctrl Pts',(-20.4566747018435,22.6469451375194,-18.6203709889245));
#32926=CARTESIAN_POINT('Ctrl Pts',(-20.4531757978372,22.6590449732178,-18.6196001628558));
#32927=CARTESIAN_POINT('Ctrl Pts',(-20.4520168098509,22.6630825258254,-18.6193428358228));
#32928=CARTESIAN_POINT('Ctrl Pts',(-20.4499747700928,22.6702491599057,-18.618885877511));
#32929=CARTESIAN_POINT('Ctrl Pts',(-20.4490885517624,22.6733773393849,-18.6186863498723));
#32930=CARTESIAN_POINT('Ctrl Pts',(-20.4473289251669,22.6796245137946,-18.6182877407046));
#32931=CARTESIAN_POINT('Ctrl Pts',(-20.4464554821057,22.6827434952383,-18.6180886605641));
#32932=CARTESIAN_POINT('Ctrl Pts',(-20.444352847166,22.6902956281589,-18.6176064481669));
#32933=CARTESIAN_POINT('Ctrl Pts',(-20.4431284452773,22.6947300962448,-18.6173231601931));
#32934=CARTESIAN_POINT('Ctrl Pts',(-20.4386189040151,22.7111998691456,-18.616270480797));
#32935=CARTESIAN_POINT('Ctrl Pts',(-20.435394196112,22.7232514762808,-18.6154991268424));
#32936=CARTESIAN_POINT('Ctrl Pts',(-20.3810804200021,22.9310617368419,-18.602179176972));
#32937=CARTESIAN_POINT('Ctrl Pts',(-20.3484763792263,23.1311455924071,-18.5890170612016));
#32938=CARTESIAN_POINT('Ctrl Pts',(-20.3149181792262,23.6276625113623,-18.5556932082558));
#32939=CARTESIAN_POINT('Ctrl Pts',(-20.3356134682672,23.923733169724,-18.5351866409336));
#32940=CARTESIAN_POINT('Ctrl Pts',(-20.3989383067089,24.2251558402493,-18.5157615024163));
#32941=CARTESIAN_POINT('Ctrl Pts',(-20.4015968617121,24.2374521422998,-18.514971911023));
#32942=CARTESIAN_POINT('Ctrl Pts',(-20.4050793761773,24.2531148139321,-18.5139700582298));
#32943=CARTESIAN_POINT('Ctrl Pts',(-20.405836806879,24.2564956313287,-18.5137540389695));
#32944=CARTESIAN_POINT('Ctrl Pts',(-20.4070593405504,24.2619114972591,-18.5134083692571));
#32945=CARTESIAN_POINT('Ctrl Pts',(-20.4075209687431,24.2639473147859,-18.5132785185702));
#32946=CARTESIAN_POINT('Ctrl Pts',(-20.4084013318278,24.2678123701854,-18.5130321589998));
#32947=CARTESIAN_POINT('Ctrl Pts',(-20.4088196832696,24.2696416772707,-18.5129156292191));
#32948=CARTESIAN_POINT('Ctrl Pts',(-20.4097812606891,24.2738294910194,-18.512649019332));
#32949=CARTESIAN_POINT('Ctrl Pts',(-20.4103255451283,24.27618774864,-18.5124990014317));
#32950=CARTESIAN_POINT('Ctrl Pts',(-20.4120091444995,24.2834450739504,-18.5120376872073));
#32951=CARTESIAN_POINT('Ctrl Pts',(-20.4131572792847,24.2883421193555,-18.511726899427));
#32952=CARTESIAN_POINT('Ctrl Pts',(-20.4218894466482,24.3251982511677,-18.5093914369112));
#32953=CARTESIAN_POINT('Ctrl Pts',(-20.4299505621905,24.3570438819683,-18.5073938027028));
#32954=CARTESIAN_POINT('Ctrl Pts',(-20.4406826865939,24.3968713803727,-18.504914693581));
#32955=CARTESIAN_POINT('Ctrl Pts',(-20.4428995474941,24.4049720945271,-18.5044114596321));
#32956=CARTESIAN_POINT('Ctrl Pts',(-20.446060058516,24.416346207733,-18.5037061690489));
#32957=CARTESIAN_POINT('Ctrl Pts',(-20.446977250674,24.4196268449872,-18.5035028935876));
#32958=CARTESIAN_POINT('Ctrl Pts',(-20.4497965758113,24.4296497709661,-18.5028822974948));
#32959=CARTESIAN_POINT('Ctrl Pts',(-20.4517155047012,24.4363873593577,-18.5024657396535));
#32960=CARTESIAN_POINT('Ctrl Pts',(-20.4552200562278,24.4485416789617,-18.5017153152276));
#32961=CARTESIAN_POINT('Ctrl Pts',(-20.4567979618975,24.4539605828386,-18.501381114507));
#32962=CARTESIAN_POINT('Ctrl Pts',(-20.5326802544959,24.712030895423,-18.4854815339245));
#32963=CARTESIAN_POINT('Ctrl Pts',(-20.6376665064033,24.9546554500305,-18.4712150431435));
#32964=CARTESIAN_POINT('Ctrl Pts',(-20.8659720275389,25.3435537016485,-18.4457478274155));
#32965=CARTESIAN_POINT('Ctrl Pts',(-20.9748410045294,25.4966672971269,-18.4349100854264));
#32966=CARTESIAN_POINT('Ctrl Pts',(-21.1017441367832,25.6457220179755,-18.4230091418124));
#32967=CARTESIAN_POINT('Ctrl Pts',(-21.1071204287556,25.6519878274655,-18.422506231955));
#32968=CARTESIAN_POINT('Ctrl Pts',(-21.1157439934182,25.6619603769088,-18.4217015628531));
#32969=CARTESIAN_POINT('Ctrl Pts',(-21.1189758181134,25.6656804761191,-18.4214004433954));
#32970=CARTESIAN_POINT('Ctrl Pts',(-21.1251430673902,25.6727466923139,-18.4208266553661));
#32971=CARTESIAN_POINT('Ctrl Pts',(-21.1280769193577,25.6760941717062,-18.4205540526225));
#32972=CARTESIAN_POINT('Ctrl Pts',(-21.1332225629593,25.6819407899663,-18.4200765559045));
#32973=CARTESIAN_POINT('Ctrl Pts',(-21.1354313240291,25.6844425970569,-18.4198717889806));
#32974=CARTESIAN_POINT('Ctrl Pts',(-21.139743820916,25.6893119859717,-18.4194723744698));
#32975=CARTESIAN_POINT('Ctrl Pts',(-21.1418471694528,25.6916799072263,-18.4192777432756));
#32976=CARTESIAN_POINT('Ctrl Pts',(-21.1468353042485,25.697278836788,-18.4188165863946));
#32977=CARTESIAN_POINT('Ctrl Pts',(-21.1497231154221,25.7005071317997,-18.4185499333667));
#32978=CARTESIAN_POINT('Ctrl Pts',(-21.1598572852436,25.7117902989115,-18.4176153053039));
#32979=CARTESIAN_POINT('Ctrl Pts',(-21.16713768669,25.7198143732358,-18.4169458906686));
#32980=CARTESIAN_POINT('Ctrl Pts',(-21.2612398816587,25.82248368211,-18.4083188457779));
#32981=CARTESIAN_POINT('Ctrl Pts',(-21.3535922850532,25.911881119943,-18.4001213143432));
#32982=CARTESIAN_POINT('Ctrl Pts',(-21.6083652100675,26.1306002489539,-18.378139209562));
#32983=CARTESIAN_POINT('Ctrl Pts',(-21.7783670839434,26.2501647503204,-18.3640416408662));
#32984=CARTESIAN_POINT('Ctrl Pts',(-21.9970129901276,26.3743472442521,-18.3470590293967));
#32985=CARTESIAN_POINT('Ctrl Pts',(-22.035816559176,26.3953442965779,-18.3440874952961));
#32986=CARTESIAN_POINT('Ctrl Pts',(-22.0750360259987,26.4155367800409,-18.341133076278));
#32987=CARTESIAN_POINT('Origin',(-23.5502525316942,23.5502525316942,-77.3107734492734));
#32988=CARTESIAN_POINT('',(-22.0750360036057,26.4155367685116,-16.8432706449041));
#32989=CARTESIAN_POINT('',(-22.0750360832114,26.4155368094973,-17.0912958973716));
#32990=CARTESIAN_POINT('',(-22.0750360153461,26.4155367745563,-77.3107734492734));
#32991=CARTESIAN_POINT('',(-26.7730012670434,23.5531887946472,-17.6894770438844));
#32992=CARTESIAN_POINT('Ctrl Pts',(-22.0750360036057,26.4155367685116,-16.8432706449041));
#32993=CARTESIAN_POINT('Ctrl Pts',(-21.96804694704,26.3604525215311,-16.8508191866373));
#32994=CARTESIAN_POINT('Ctrl Pts',(-21.8642302636496,26.2994208678429,-16.8585779079896));
#32995=CARTESIAN_POINT('Ctrl Pts',(-21.5633378707484,26.099065331876,-16.8823973090096));
#32996=CARTESIAN_POINT('Ctrl Pts',(-21.3782495467658,25.9432968497533,-16.8989554479486));
#32997=CARTESIAN_POINT('Ctrl Pts',(-21.1808597702974,25.7352424798406,-16.9181188309119));
#32998=CARTESIAN_POINT('Ctrl Pts',(-21.1501344007855,25.701446712473,-16.9211496604168));
#32999=CARTESIAN_POINT('Ctrl Pts',(-21.0959682993008,25.6392619682466,-16.9265650425278));
#33000=CARTESIAN_POINT('Ctrl Pts',(-21.0722758943645,25.6111027284705,-16.9289603448162));
#33001=CARTESIAN_POINT('Ctrl Pts',(-21.0247681712526,25.5526339692323,-16.9338085687613));
#33002=CARTESIAN_POINT('Ctrl Pts',(-21.0010033897433,25.5222900105741,-16.9362585083589));
#33003=CARTESIAN_POINT('Ctrl Pts',(-20.9749289354075,25.4877376168091,-16.9389680688449));
#33004=CARTESIAN_POINT('Ctrl Pts',(-20.9720788623098,25.4839434614478,-16.9392645347807));
#33005=CARTESIAN_POINT('Ctrl Pts',(-20.9677979087803,25.4782181588588,-16.939710272599));
#33006=CARTESIAN_POINT('Ctrl Pts',(-20.9663608071792,25.476291704456,-16.9398599788844));
#33007=CARTESIAN_POINT('Ctrl Pts',(-20.9638747984296,25.4729513855323,-16.9401190773998));
#33008=CARTESIAN_POINT('Ctrl Pts',(-20.9628248949125,25.4715382694568,-16.9402285399604));
#33009=CARTESIAN_POINT('Ctrl Pts',(-20.9606389506813,25.4685910595728,-16.940456525414));
#33010=CARTESIAN_POINT('Ctrl Pts',(-20.9595031162403,25.4670568182227,-16.9405750333541));
#33011=CARTESIAN_POINT('Ctrl Pts',(-20.9572447703715,25.4640006573558,-16.9408107503835));
#33012=CARTESIAN_POINT('Ctrl Pts',(-20.9561222326798,25.4624787553751,-16.9409279613844));
#33013=CARTESIAN_POINT('Ctrl Pts',(-20.9522620661767,25.4572356060327,-16.9413311835222));
#33014=CARTESIAN_POINT('Ctrl Pts',(-20.9495310829099,25.4535094379466,-16.9416167296418));
#33015=CARTESIAN_POINT('Ctrl Pts',(-20.9269107289283,25.4225065086866,-16.9439842800525));
#33016=CARTESIAN_POINT('Ctrl Pts',(-20.9074421058048,25.3949233540039,-16.9460375037073));
#33017=CARTESIAN_POINT('Ctrl Pts',(-20.8386717953634,25.2941653038298,-16.9533676938207));
#33018=CARTESIAN_POINT('Ctrl Pts',(-20.7919431031212,25.2192742892847,-16.9584986188464));
#33019=CARTESIAN_POINT('Ctrl Pts',(-20.6504257555518,24.9702518474096,-16.9748694763735));
#33020=CARTESIAN_POINT('Ctrl Pts',(-20.5686070458863,24.7892803981913,-16.9857434101372));
#33021=CARTESIAN_POINT('Ctrl Pts',(-20.4426548413835,24.4244441448356,-17.0075353906023));
#33022=CARTESIAN_POINT('Ctrl Pts',(-20.3970179391443,24.2419678355796,-17.018381759352));
#33023=CARTESIAN_POINT('Ctrl Pts',(-20.365573583826,24.044308993587,-17.0305452570156));
#33024=CARTESIAN_POINT('Ctrl Pts',(-20.3636934196434,24.0320334021841,-17.0313022108979));
#33025=CARTESIAN_POINT('Ctrl Pts',(-20.3612153948387,24.0152049841527,-17.0323421107643));
#33026=CARTESIAN_POINT('Ctrl Pts',(-20.3605562263855,24.0106611793497,-17.032623111525));
#33027=CARTESIAN_POINT('Ctrl Pts',(-20.3594489787931,24.0029121428463,-17.0331027120925));
#33028=CARTESIAN_POINT('Ctrl Pts',(-20.3589960123647,23.9997076067543,-17.0333011567648));
#33029=CARTESIAN_POINT('Ctrl Pts',(-20.3581277515499,23.9934975610663,-17.0336859376894));
#33030=CARTESIAN_POINT('Ctrl Pts',(-20.3577118727966,23.9904921360718,-17.0338722551661));
#33031=CARTESIAN_POINT('Ctrl Pts',(-20.3567328343199,23.9833425869162,-17.0343157179243));
#33032=CARTESIAN_POINT('Ctrl Pts',(-20.3561734971423,23.9791979527247,-17.0345729839876));
#33033=CARTESIAN_POINT('Ctrl Pts',(-20.3545528916947,23.9670104795249,-17.03533004539));
#33034=CARTESIAN_POINT('Ctrl Pts',(-20.3535139288785,23.9589647525921,-17.0358305459737));
#33035=CARTESIAN_POINT('Ctrl Pts',(-20.3456798904373,23.8964401570158,-17.0397256913232));
#33036=CARTESIAN_POINT('Ctrl Pts',(-20.340247903784,23.8418024812624,-17.0431631955353));
#33037=CARTESIAN_POINT('Ctrl Pts',(-20.3265403901067,23.6557553758703,-17.0549926988762));
#33038=CARTESIAN_POINT('Ctrl Pts',(-20.3249224193299,23.5240019232793,-17.0635868173886));
#33039=CARTESIAN_POINT('Ctrl Pts',(-20.340012973357,23.216021887351,-17.0841202573986));
#33040=CARTESIAN_POINT('Ctrl Pts',(-20.3631656999452,23.0405268389459,-17.0961726180614));
#33041=CARTESIAN_POINT('Ctrl Pts',(-20.4311993539924,22.7265239113891,-17.1177944931616));
#33042=CARTESIAN_POINT('Ctrl Pts',(-20.4712936712857,22.5874207338688,-17.1273862976394));
#33043=CARTESIAN_POINT('Ctrl Pts',(-20.5237631528781,22.4427483184868,-17.13706344723));
#33044=CARTESIAN_POINT('Ctrl Pts',(-20.5269622483884,22.4340449299208,-17.1376444115209));
#33045=CARTESIAN_POINT('Ctrl Pts',(-20.531319261265,22.4223474942285,-17.1384234897314));
#33046=CARTESIAN_POINT('Ctrl Pts',(-20.5324441114198,22.4193413045942,-17.138623554));
#33047=CARTESIAN_POINT('Ctrl Pts',(-20.5342165065292,22.4146260096051,-17.1389371108304));
#33048=CARTESIAN_POINT('Ctrl Pts',(-20.5348610134828,22.4129157765051,-17.1390507859801));
#33049=CARTESIAN_POINT('Ctrl Pts',(-20.5361035694441,22.4096270694643,-17.1392692779407));
#33050=CARTESIAN_POINT('Ctrl Pts',(-20.5367013997857,22.4080485275388,-17.1393741067806));
#33051=CARTESIAN_POINT('Ctrl Pts',(-20.5381229949944,22.4043037598441,-17.1396226862725));
#33052=CARTESIAN_POINT('Ctrl Pts',(-20.5389478557297,22.4021379545899,-17.1397663698265));
#33053=CARTESIAN_POINT('Ctrl Pts',(-20.541357039018,22.3958327113567,-17.1401844329048));
#33054=CARTESIAN_POINT('Ctrl Pts',(-20.5429475737639,22.3916956284733,-17.1404584385661));
#33055=CARTESIAN_POINT('Ctrl Pts',(-20.5548018470508,22.3610507989383,-17.1424859649064));
#33056=CARTESIAN_POINT('Ctrl Pts',(-20.5654077729336,22.3346755222715,-17.1442191818706));
#33057=CARTESIAN_POINT('Ctrl Pts',(-20.6017292012615,22.247692813452,-17.1499066817369));
#33058=CARTESIAN_POINT('Ctrl Pts',(-20.6289540819225,22.1877297734362,-17.153781279089));
#33059=CARTESIAN_POINT('Ctrl Pts',(-20.7372658994601,21.9673708566774,-17.1679965221193));
#33060=CARTESIAN_POINT('Ctrl Pts',(-20.8298874308516,21.8130044935711,-17.1779212820264));
#33061=CARTESIAN_POINT('Ctrl Pts',(-21.0697770029897,21.4798321146654,-17.2009104912029));
#33062=CARTESIAN_POINT('Ctrl Pts',(-21.2243639869269,21.3075713596742,-17.2140341460924));
#33063=CARTESIAN_POINT('Ctrl Pts',(-21.407173196034,21.1432722858051,-17.2289467389562));
#33064=CARTESIAN_POINT('Ctrl Pts',(-21.4184088251431,21.13331534965,-17.229860817));
#33065=CARTESIAN_POINT('Ctrl Pts',(-21.4338731860062,21.1198026675201,-17.2311157467339));
#33066=CARTESIAN_POINT('Ctrl Pts',(-21.4380422232875,21.1161786442416,-17.231453750464));
#33067=CARTESIAN_POINT('Ctrl Pts',(-21.4446679149906,21.1104489631132,-17.2319904410409));
#33068=CARTESIAN_POINT('Ctrl Pts',(-21.4471184716641,21.1083362438626,-17.2321888347765));
#33069=CARTESIAN_POINT('Ctrl Pts',(-21.4518733433731,21.1042493526764,-17.2325735818699));
#33070=CARTESIAN_POINT('Ctrl Pts',(-21.4541772740624,21.1022747368623,-17.2327599166013));
#33071=CARTESIAN_POINT('Ctrl Pts',(-21.4596648744836,21.0975849394553,-17.2332035223859));
#33072=CARTESIAN_POINT('Ctrl Pts',(-21.4628510441962,21.0948727035968,-17.2334609144467));
#33073=CARTESIAN_POINT('Ctrl Pts',(-21.4694597672096,21.0892691698485,-17.2339944456541));
#33074=CARTESIAN_POINT('Ctrl Pts',(-21.4728830841221,21.0863787902088,-17.2342706217937));
#33075=CARTESIAN_POINT('Ctrl Pts',(-21.492359883828,21.0700035586344,-17.235840834072));
#33076=CARTESIAN_POINT('Ctrl Pts',(-21.5085383256254,21.0566687280514,-17.2371409867368));
#33077=CARTESIAN_POINT('Ctrl Pts',(-21.5512427408478,21.0221644912691,-17.2405626831116));
#33078=CARTESIAN_POINT('Ctrl Pts',(-21.5779744559629,21.0012550161763,-17.2426944903578));
#33079=CARTESIAN_POINT('Ctrl Pts',(-21.6996767922388,20.9091204109294,-17.2523581312154));
#33080=CARTESIAN_POINT('Ctrl Pts',(-21.7981990149075,20.842760632787,-17.2600734043017));
#33081=CARTESIAN_POINT('Ctrl Pts',(-22.033301404395,20.7026207861129,-17.2782136140443));
#33082=CARTESIAN_POINT('Ctrl Pts',(-22.1720017570271,20.6329649998257,-17.2887274587443));
#33083=CARTESIAN_POINT('Ctrl Pts',(-22.4308285575074,20.5255725859626,-17.3076802213987));
#33084=CARTESIAN_POINT('Ctrl Pts',(-22.549199646221,20.4843601060258,-17.3161103330227));
#33085=CARTESIAN_POINT('Ctrl Pts',(-22.6748546029482,20.4486682578361,-17.3246370894903));
#33086=CARTESIAN_POINT('Ctrl Pts',(-22.680036676437,20.4472103296837,-17.3249879944401));
#33087=CARTESIAN_POINT('Ctrl Pts',(-22.6905340072655,20.4442853675455,-17.3256972884426));
#33088=CARTESIAN_POINT('Ctrl Pts',(-22.6958494286436,20.4428189758001,-17.3260556513625));
#33089=CARTESIAN_POINT('Ctrl Pts',(-22.7107655350814,20.4387451613446,-17.3270590124645));
#33090=CARTESIAN_POINT('Ctrl Pts',(-22.7203746521251,20.4361685182054,-17.3277027496838));
#33091=CARTESIAN_POINT('Ctrl Pts',(-22.7316890351813,20.433190705099,-17.3284575075749));
#33092=CARTESIAN_POINT('Ctrl Pts',(-22.7333827737537,20.432746408649,-17.3285704084954));
#33093=CARTESIAN_POINT('Ctrl Pts',(-22.7743444358782,20.4220371413395,-17.3312987626036));
#33094=CARTESIAN_POINT('Ctrl Pts',(-22.8138047610682,20.4125129049238,-17.3338813594173));
#33095=CARTESIAN_POINT('Ctrl Pts',(-22.8585920405919,20.4025944802969,-17.3367530450246));
#33096=CARTESIAN_POINT('Ctrl Pts',(-22.8637502232173,20.4014654596809,-17.3370828908535));
#33097=CARTESIAN_POINT('Ctrl Pts',(-22.8713353541448,20.3998247543918,-17.3375666021878));
#33098=CARTESIAN_POINT('Ctrl Pts',(-22.8737601217602,20.3993031932612,-17.3377210327133));
#33099=CARTESIAN_POINT('Ctrl Pts',(-22.8780346559443,20.3983889137949,-17.337992918496));
#33100=CARTESIAN_POINT('Ctrl Pts',(-22.8798841677855,20.3979950239611,-17.3381104416108));
#33101=CARTESIAN_POINT('Ctrl Pts',(-22.8837275527096,20.397180035273,-17.3383544170978));
#33102=CARTESIAN_POINT('Ctrl Pts',(-22.8857214749929,20.3967592004767,-17.3384808539184));
#33103=CARTESIAN_POINT('Ctrl Pts',(-22.8897616608319,20.3959104858391,-17.3387367735365));
#33104=CARTESIAN_POINT('Ctrl Pts',(-22.8918079445305,20.395482705156,-17.3388662505562));
#33105=CARTESIAN_POINT('Ctrl Pts',(-22.8998270433523,20.393814434748,-17.3393731024957));
#33106=CARTESIAN_POINT('Ctrl Pts',(-22.9058030101936,20.3925889030892,-17.3397496212549));
#33107=CARTESIAN_POINT('Ctrl Pts',(-23.0043178110267,20.3726771288172,-17.3459374434307));
#33108=CARTESIAN_POINT('Ctrl Pts',(-23.0976409194408,20.3580468877669,-17.351521241554));
#33109=CARTESIAN_POINT('Ctrl Pts',(-23.3390432656529,20.3310048111058,-17.3655639843818));
#33110=CARTESIAN_POINT('Ctrl Pts',(-23.4875802407342,20.3246916601377,-17.3738269725923));
#33111=CARTESIAN_POINT('Ctrl Pts',(-23.7963756034704,20.3329136186268,-17.391089225246));
#33112=CARTESIAN_POINT('Ctrl Pts',(-23.9561698241481,20.3491476900238,-17.4000750001182));
#33113=CARTESIAN_POINT('Ctrl Pts',(-24.1481326698673,20.3832582173666,-17.4113942252007));
#33114=CARTESIAN_POINT('Ctrl Pts',(-24.1820832267468,20.3898564329187,-17.4134157812549));
#33115=CARTESIAN_POINT('Ctrl Pts',(-24.2863502877249,20.4118677378608,-17.4196931617098));
#33116=CARTESIAN_POINT('Ctrl Pts',(-24.3562578225558,20.4290903657804,-17.423999651768));
#33117=CARTESIAN_POINT('Ctrl Pts',(-24.434719751617,20.4512322753629,-17.4289649146538));
#33118=CARTESIAN_POINT('Ctrl Pts',(-24.4439015124666,20.4538674929203,-17.4295480154675));
#33119=CARTESIAN_POINT('Ctrl Pts',(-24.4572956640277,20.4577762289306,-17.4304016828261));
#33120=CARTESIAN_POINT('Ctrl Pts',(-24.4615174374266,20.4590176330908,-17.4306711988149));
#33121=CARTESIAN_POINT('Ctrl Pts',(-24.4689853690408,20.4612301917346,-17.43114873944));
#33122=CARTESIAN_POINT('Ctrl Pts',(-24.4722325697174,20.4621978280765,-17.4313566485794));
#33123=CARTESIAN_POINT('Ctrl Pts',(-24.4789637907268,20.4642152343999,-17.4317881827261));
#33124=CARTESIAN_POINT('Ctrl Pts',(-24.4824475697235,20.4652657871772,-17.4320118331544));
#33125=CARTESIAN_POINT('Ctrl Pts',(-24.4914048405004,20.4679834596311,-17.4325876645351));
#33126=CARTESIAN_POINT('Ctrl Pts',(-24.4968756680402,20.4696592547382,-17.4329401299383));
#33127=CARTESIAN_POINT('Ctrl Pts',(-24.5086808465571,20.4733097712065,-17.4337023600789));
#33128=CARTESIAN_POINT('Ctrl Pts',(-24.5150136104179,20.4752895000512,-17.4341122884583));
#33129=CARTESIAN_POINT('Ctrl Pts',(-24.5640902599528,20.4907982178886,-17.4372972083485));
#33130=CARTESIAN_POINT('Ctrl Pts',(-24.6065519239492,20.5051977039566,-17.4401007952553));
#33131=CARTESIAN_POINT('Ctrl Pts',(-24.74547229614,20.5555633003076,-17.4494380162596));
#33132=CARTESIAN_POINT('Ctrl Pts',(-24.8405007964626,20.5952619060911,-17.4560931892079));
#33133=CARTESIAN_POINT('Ctrl Pts',(-25.0062329707142,20.6740170766408,-17.4681777336673));
#33134=CARTESIAN_POINT('Ctrl Pts',(-25.0776802754617,20.7113138777421,-17.4735545408708));
#33135=CARTESIAN_POINT('Ctrl Pts',(-25.2142658345626,20.7892635755675,-17.4841314241855));
#33136=CARTESIAN_POINT('Ctrl Pts',(-25.2795005427411,20.8296457565682,-17.4893242238635));
#33137=CARTESIAN_POINT('Ctrl Pts',(-25.4638365354826,20.953065598104,-17.5043400411272));
#33138=CARTESIAN_POINT('Ctrl Pts',(-25.5788577619415,21.0418764631769,-17.5141492582854));
#33139=CARTESIAN_POINT('Ctrl Pts',(-25.6935130119421,21.1434670236394,-17.524136936191));
#33140=CARTESIAN_POINT('Ctrl Pts',(-25.6994998051523,21.1488116875558,-17.5246590669108));
#33141=CARTESIAN_POINT('Ctrl Pts',(-25.7443728087281,21.1891739371715,-17.5285768787183));
#33142=CARTESIAN_POINT('Ctrl Pts',(-25.7824237520687,21.2251141803083,-17.5319233599273));
#33143=CARTESIAN_POINT('Ctrl Pts',(-25.8236561060968,21.2660050355662,-17.535560355957));
#33144=CARTESIAN_POINT('Ctrl Pts',(-25.827716392031,21.2700532417767,-17.5359186207287));
#33145=CARTESIAN_POINT('Ctrl Pts',(-25.8333894611651,21.27573970293,-17.536419328156));
#33146=CARTESIAN_POINT('Ctrl Pts',(-25.8350112968492,21.2773688496605,-17.5365624877546));
#33147=CARTESIAN_POINT('Ctrl Pts',(-25.8379758026856,21.2803530984839,-17.5368241913237));
#33148=CARTESIAN_POINT('Ctrl Pts',(-25.8393190146191,21.2817076592414,-17.5369427786302));
#33149=CARTESIAN_POINT('Ctrl Pts',(-25.8420450773319,21.2844616408839,-17.5371834714584));
#33150=CARTESIAN_POINT('Ctrl Pts',(-25.8434278497673,21.2858611358111,-17.5373055707346));
#33151=CARTESIAN_POINT('Ctrl Pts',(-25.8462036552274,21.2886756606445,-17.5375506973321));
#33152=CARTESIAN_POINT('Ctrl Pts',(-25.8475966637942,21.2900907135765,-17.5376737226982));
#33153=CARTESIAN_POINT('Ctrl Pts',(-25.8509391731548,21.2934924009907,-17.5379689503513));
#33154=CARTESIAN_POINT('Ctrl Pts',(-25.8528874140144,21.2954802796499,-17.5381410532511));
#33155=CARTESIAN_POINT('Ctrl Pts',(-25.8667138213189,21.3096246005948,-17.5393626392026));
#33156=CARTESIAN_POINT('Ctrl Pts',(-25.8784985318812,21.3218726214436,-17.5404048595836));
#33157=CARTESIAN_POINT('Ctrl Pts',(-25.9787338810159,21.4277119440664,-17.5492844128103));
#33158=CARTESIAN_POINT('Ctrl Pts',(-26.0616097220952,21.5264458220591,-17.5567285263041));
#33159=CARTESIAN_POINT('Ctrl Pts',(-26.1639331037628,21.6643487877935,-17.5664634220971));
#33160=CARTESIAN_POINT('Ctrl Pts',(-26.1888134171712,21.6993188101822,-17.568879186385));
#33161=CARTESIAN_POINT('Ctrl Pts',(-26.2381809917884,21.771725581756,-17.5737955040987));
#33162=CARTESIAN_POINT('Ctrl Pts',(-26.2626019947166,21.8091959672489,-17.5762948004595));
#33163=CARTESIAN_POINT('Ctrl Pts',(-26.4286473133635,22.0759447483404,-17.5938515949625));
#33164=CARTESIAN_POINT('Ctrl Pts',(-26.5417804183748,22.3216457388228,-17.6089401347476));
#33165=CARTESIAN_POINT('Ctrl Pts',(-26.6282426640411,22.5950591688404,-17.6263134833063));
#33166=CARTESIAN_POINT('Ctrl Pts',(-26.6333322020503,22.6116166367759,-17.6273672319988));
#33167=CARTESIAN_POINT('Ctrl Pts',(-26.6399642398489,22.6338282566221,-17.6287832823414));
#33168=CARTESIAN_POINT('Ctrl Pts',(-26.6416252212874,22.6394469625577,-17.6291416995508));
#33169=CARTESIAN_POINT('Ctrl Pts',(-26.6441984180381,22.6482396045388,-17.6297029203342));
#33170=CARTESIAN_POINT('Ctrl Pts',(-26.6451210983771,22.6514104859446,-17.6299053814626));
#33171=CARTESIAN_POINT('Ctrl Pts',(-26.646877599503,22.657481643505,-17.6302931591227));
#33172=CARTESIAN_POINT('Ctrl Pts',(-26.6477122240757,22.6603816852491,-17.6304784491741));
#33173=CARTESIAN_POINT('Ctrl Pts',(-26.6496553301233,22.6671691852948,-17.6309122557648));
#33174=CARTESIAN_POINT('Ctrl Pts',(-26.6507605712623,22.6710575590427,-17.6311608777462));
#33175=CARTESIAN_POINT('Ctrl Pts',(-26.653021987363,22.6790707947807,-17.6316734651046));
#33176=CARTESIAN_POINT('Ctrl Pts',(-26.6541772590579,22.6831959012837,-17.631937459399));
#33177=CARTESIAN_POINT('Ctrl Pts',(-26.6571229753068,22.6937954497064,-17.6326161152338));
#33178=CARTESIAN_POINT('Ctrl Pts',(-26.6589014013733,22.7002731845175,-17.6330311675787));
#33179=CARTESIAN_POINT('Ctrl Pts',(-26.6733009722911,22.7533718584892,-17.6364359452005));
#33180=CARTESIAN_POINT('Ctrl Pts',(-26.6848922723432,22.80026342731,-17.6394589367402));
#33181=CARTESIAN_POINT('Ctrl Pts',(-26.7472119689281,23.079134187124,-17.6575448897184));
#33182=CARTESIAN_POINT('Ctrl Pts',(-26.773217394735,23.3158359840599,-17.673413816263));
#33183=CARTESIAN_POINT('Ctrl Pts',(-26.7730011947243,23.5531880789698,-17.6894771219796));
#33184=CARTESIAN_POINT('Ctrl Pts',(-26.7730011940801,23.5531887860566,-17.6894771698332));
#33185=CARTESIAN_POINT('Ctrl Pts',(-26.7728035334531,23.7701354272215,-17.7041594933754));
#33186=CARTESIAN_POINT('Ctrl Pts',(-26.750700095684,23.9865403688873,-17.7189048342478));
#33187=CARTESIAN_POINT('Ctrl Pts',(-26.7054279707792,24.2067942912656,-17.7330769488637));
#33188=CARTESIAN_POINT('Ctrl Pts',(-26.703820059033,24.2144746232993,-17.7335700142139));
#33189=CARTESIAN_POINT('Ctrl Pts',(-26.7013473410846,24.2260743815403,-17.7343129250898));
#33190=CARTESIAN_POINT('Ctrl Pts',(-26.700503252243,24.2299981227726,-17.7345639150239));
#33191=CARTESIAN_POINT('Ctrl Pts',(-26.699121999286,24.236361033653,-17.7349704207056));
#33192=CARTESIAN_POINT('Ctrl Pts',(-26.698589328965,24.2388011584762,-17.735126190413));
#33193=CARTESIAN_POINT('Ctrl Pts',(-26.6975549418408,24.243513316233,-17.7354267604997));
#33194=CARTESIAN_POINT('Ctrl Pts',(-26.697053600321,24.245785428735,-17.7355715822987));
#33195=CARTESIAN_POINT('Ctrl Pts',(-26.6961492433367,24.249863040753,-17.7358312892841));
#33196=CARTESIAN_POINT('Ctrl Pts',(-26.6957471348637,24.2516687321048,-17.735946226568));
#33197=CARTESIAN_POINT('Ctrl Pts',(-26.6948765312281,24.2555624233151,-17.7361939218202));
#33198=CARTESIAN_POINT('Ctrl Pts',(-26.694407512394,24.2576502975004,-17.7363266487428));
#33199=CARTESIAN_POINT('Ctrl Pts',(-26.6931425309738,24.2632553500378,-17.7366827202205));
#33200=CARTESIAN_POINT('Ctrl Pts',(-26.6923427410553,24.2667716752463,-17.7369058435285));
#33201=CARTESIAN_POINT('Ctrl Pts',(-26.6886742590934,24.2827761185761,-17.7379202384871));
#33202=CARTESIAN_POINT('Ctrl Pts',(-26.6857369557167,24.2952486283448,-17.7387075995406));
#33203=CARTESIAN_POINT('Ctrl Pts',(-26.6325100435688,24.5153709223802,-17.7525526223934));
#33204=CARTESIAN_POINT('Ctrl Pts',(-26.5617591528579,24.7175671545417,-17.7644892674023));
#33205=CARTESIAN_POINT('Ctrl Pts',(-26.4514109483188,24.9544105521194,-17.7790919781919));
#33206=CARTESIAN_POINT('Ctrl Pts',(-26.4303715395265,24.9970746987324,-17.7817475530847));
#33207=CARTESIAN_POINT('Ctrl Pts',(-26.3864584058268,25.0813659080866,-17.7870688223549));
#33208=CARTESIAN_POINT('Ctrl Pts',(-26.3635935689955,25.1229839214066,-17.7897338211128));
#33209=CARTESIAN_POINT('Ctrl Pts',(-26.2717749514428,25.2816959764744,-17.8000854151909));
#33210=CARTESIAN_POINT('Ctrl Pts',(-26.1963685145398,25.3948785722305,-17.8078795774982));
#33211=CARTESIAN_POINT('Ctrl Pts',(-26.0803588544134,25.5471930432055,-17.8192351448813));
#33212=CARTESIAN_POINT('Ctrl Pts',(-26.0455299702784,25.5905464661932,-17.8225740260591));
#33213=CARTESIAN_POINT('Ctrl Pts',(-26.005028931909,25.6383713948799,-17.8263889033132));
#33214=CARTESIAN_POINT('Ctrl Pts',(-26.00044152117,25.6437523469423,-17.8268200545638));
#33215=CARTESIAN_POINT('Ctrl Pts',(-25.9929495705041,25.6524819169802,-17.8275226780766));
#33216=CARTESIAN_POINT('Ctrl Pts',(-25.9900557482718,25.6558397362144,-17.8277937075588));
#33217=CARTESIAN_POINT('Ctrl Pts',(-25.9844393862448,25.6623295049565,-17.8283190270339));
#33218=CARTESIAN_POINT('Ctrl Pts',(-25.9817177052509,25.6654621887675,-17.8285732811022));
#33219=CARTESIAN_POINT('Ctrl Pts',(-25.9769984613108,25.6708729445602,-17.8290136038822));
#33220=CARTESIAN_POINT('Ctrl Pts',(-25.9750037178381,25.673153477939,-17.8291995548565));
#33221=CARTESIAN_POINT('Ctrl Pts',(-25.9708625323528,25.6778745259783,-17.8295852567235));
#33222=CARTESIAN_POINT('Ctrl Pts',(-25.9687156092587,25.6803146125233,-17.8297850276312));
#33223=CARTESIAN_POINT('Ctrl Pts',(-25.9628610868698,25.6869483113336,-17.8303292786548));
#33224=CARTESIAN_POINT('Ctrl Pts',(-25.9591462598095,25.6911355040328,-17.8306740618876));
#33225=CARTESIAN_POINT('Ctrl Pts',(-25.9451054690054,25.7068788651299,-17.8319751549206));
#33226=CARTESIAN_POINT('Ctrl Pts',(-25.9347072325416,25.7183700330137,-17.8329345109604));
#33227=CARTESIAN_POINT('Ctrl Pts',(-25.7647938320869,25.903441791644,-17.8485450138293));
#33228=CARTESIAN_POINT('Ctrl Pts',(-25.5868230700623,26.0590431341482,-17.8640432729725));
#33229=CARTESIAN_POINT('Ctrl Pts',(-25.3716960621877,26.209043404578,-17.8817262533506));
#33230=CARTESIAN_POINT('Ctrl Pts',(-25.3496841183654,26.2239898760536,-17.8835234858929));
#33231=CARTESIAN_POINT('Ctrl Pts',(-25.2363760842775,26.2988948571337,-17.8927083679957));
#33232=CARTESIAN_POINT('Ctrl Pts',(-25.1422580262028,26.3544576793462,-17.9001229345794));
#33233=CARTESIAN_POINT('Ctrl Pts',(-24.9600283072215,26.449900627059,-17.913907583769));
#33234=CARTESIAN_POINT('Ctrl Pts',(-24.8725820426677,26.4908094153954,-17.9202911940178));
#33235=CARTESIAN_POINT('Ctrl Pts',(-24.7509725740385,26.5411759226895,-17.9287417151288));
#33236=CARTESIAN_POINT('Ctrl Pts',(-24.7183012032523,26.5540857334741,-17.9309711779779));
#33237=CARTESIAN_POINT('Ctrl Pts',(-24.6821253946209,26.5677007589501,-17.9333900180984));
#33238=CARTESIAN_POINT('Ctrl Pts',(-24.6788250694092,26.5689366836709,-17.9336102368542));
#33239=CARTESIAN_POINT('Ctrl Pts',(-24.6733746801333,26.5709675888983,-17.9339731674107));
#33240=CARTESIAN_POINT('Ctrl Pts',(-24.6712257939587,26.5717656894515,-17.9341160642425));
#33241=CARTESIAN_POINT('Ctrl Pts',(-24.6670320090291,26.5733181797033,-17.934394563579));
#33242=CARTESIAN_POINT('Ctrl Pts',(-24.6649871935428,26.5740727887383,-17.9345301791998));
#33243=CARTESIAN_POINT('Ctrl Pts',(-24.6613676932683,26.5754043415516,-17.9347699177233));
#33244=CARTESIAN_POINT('Ctrl Pts',(-24.6597933320916,26.5759821275511,-17.9348740911488));
#33245=CARTESIAN_POINT('Ctrl Pts',(-24.6564246109142,26.5772154556602,-17.9350967711779));
#33246=CARTESIAN_POINT('Ctrl Pts',(-24.6546301239791,26.5778706294102,-17.935215255227));
#33247=CARTESIAN_POINT('Ctrl Pts',(-24.6494332596186,26.5797627885037,-17.935557997589));
#33248=CARTESIAN_POINT('Ctrl Pts',(-24.6460293650796,26.5809956419686,-17.9357820074977));
#33249=CARTESIAN_POINT('Ctrl Pts',(-24.6308131773084,26.5864777934003,-17.9367812573661));
#33250=CARTESIAN_POINT('Ctrl Pts',(-24.6189779848573,26.5906638635103,-17.9375527591955));
#33251=CARTESIAN_POINT('Ctrl Pts',(-24.4161254700783,26.6610813091487,-17.9506834035905));
#33252=CARTESIAN_POINT('Ctrl Pts',(-24.2192839323799,26.7092738162329,-17.9620366300861));
#33253=CARTESIAN_POINT('Ctrl Pts',(-23.8489258161291,26.763744577359,-17.9829719347536));
#33254=CARTESIAN_POINT('Ctrl Pts',(-23.6769269959545,26.77510703349,-17.9925349779485));
#33255=CARTESIAN_POINT('Ctrl Pts',(-23.392971874663,26.7711064833021,-18.008891086484));
#33256=CARTESIAN_POINT('Ctrl Pts',(-23.2812599049993,26.7637049200551,-18.0154671849132));
#33257=CARTESIAN_POINT('Ctrl Pts',(-23.1490820364862,26.74800653137,-18.0235144916919));
#33258=CARTESIAN_POINT('Ctrl Pts',(-23.1280227536391,26.7452940634512,-18.0248046057233));
#33259=CARTESIAN_POINT('Ctrl Pts',(-23.1025383600989,26.7417552815286,-18.0263759263683));
#33260=CARTESIAN_POINT('Ctrl Pts',(-23.0980858416614,26.7411275003744,-18.0266508352648));
#33261=CARTESIAN_POINT('Ctrl Pts',(-23.0894810167038,26.7398958941639,-18.027182848125));
#33262=CARTESIAN_POINT('Ctrl Pts',(-23.0853285447567,26.7392932738109,-18.0274399134497));
#33263=CARTESIAN_POINT('Ctrl Pts',(-23.0781736617958,26.7382406621713,-18.0278834196943));
#33264=CARTESIAN_POINT('Ctrl Pts',(-23.0751706806876,26.7377945336463,-18.0280697377896));
#33265=CARTESIAN_POINT('Ctrl Pts',(-23.0689732858832,26.7368648846715,-18.0284546118971));
#33266=CARTESIAN_POINT('Ctrl Pts',(-23.0657789607793,26.7363808027408,-18.0286531855597));
#33267=CARTESIAN_POINT('Ctrl Pts',(-23.057148814067,26.7350596742105,-18.0291902120993));
#33268=CARTESIAN_POINT('Ctrl Pts',(-23.0517144165878,26.7342135174079,-18.0295289540927));
#33269=CARTESIAN_POINT('Ctrl Pts',(-23.0316095850853,26.7310303830804,-18.0307843009646));
#33270=CARTESIAN_POINT('Ctrl Pts',(-23.0169533713841,26.7286059166507,-18.0317036838377));
#33271=CARTESIAN_POINT('Ctrl Pts',(-22.7629733867044,26.684785763111,-18.0477110970093));
#33272=CARTESIAN_POINT('Ctrl Pts',(-22.5291197751893,26.6165773670986,-18.0637028269546));
#33273=CARTESIAN_POINT('Ctrl Pts',(-22.227063604625,26.4900591572379,-18.0858020752168));
#33274=CARTESIAN_POINT('Ctrl Pts',(-22.1502873850307,26.4542806029891,-18.0915453905923));
#33275=CARTESIAN_POINT('Ctrl Pts',(-22.0750358296283,26.4155366789378,-18.0972636326348));
#33276=CARTESIAN_POINT('Ctrl Pts',(-22.0750360259987,26.4155367800409,-18.341133076278));
#33277=CARTESIAN_POINT('Ctrl Pts',(-22.1107494798326,26.4339241622357,-18.3384427667008));
#33278=CARTESIAN_POINT('Ctrl Pts',(-22.1468077974856,26.4516443954618,-18.3357666641265));
#33279=CARTESIAN_POINT('Ctrl Pts',(-22.2398433215542,26.495224313223,-18.3289790137113));
#33280=CARTESIAN_POINT('Ctrl Pts',(-22.2972591835044,26.520107725815,-18.3248999815242));
#33281=CARTESIAN_POINT('Ctrl Pts',(-22.3812604016217,26.5536426650787,-18.3191249420596));
#33282=CARTESIAN_POINT('Ctrl Pts',(-22.4072880474223,26.5636438455556,-18.3173617455498));
#33283=CARTESIAN_POINT('Ctrl Pts',(-22.437593091106,26.5748394626856,-18.3153416885302));
#33284=CARTESIAN_POINT('Ctrl Pts',(-22.4417460973369,26.5763640001303,-18.3150655712501));
#33285=CARTESIAN_POINT('Ctrl Pts',(-22.4480601401913,26.5786670955536,-18.3146468696084));
#33286=CARTESIAN_POINT('Ctrl Pts',(-22.4502188702196,26.5794518949228,-18.3145039123284));
#33287=CARTESIAN_POINT('Ctrl Pts',(-22.4541320335498,26.5808697782033,-18.3142451254041));
#33288=CARTESIAN_POINT('Ctrl Pts',(-22.4558861719905,26.5815036450292,-18.3141292489129));
#33289=CARTESIAN_POINT('Ctrl Pts',(-22.459681324592,26.5828713189604,-18.3138788241553));
#33290=CARTESIAN_POINT('Ctrl Pts',(-22.4617225238618,26.5836045865594,-18.313744308768));
#33291=CARTESIAN_POINT('Ctrl Pts',(-22.4672761975808,26.5855933257188,-18.3133787898246));
#33292=CARTESIAN_POINT('Ctrl Pts',(-22.4707901277886,26.5868447655985,-18.3131480280056));
#33293=CARTESIAN_POINT('Ctrl Pts',(-22.4875113190866,26.592767104514,-18.3120523259615));
#33294=CARTESIAN_POINT('Ctrl Pts',(-22.5007470330634,26.5973580493987,-18.3111920981217));
#33295=CARTESIAN_POINT('Ctrl Pts',(-22.5160201263872,26.6025443574281,-18.3102071309731));
#33296=CARTESIAN_POINT('Ctrl Pts',(-22.5180283853333,26.6032240954885,-18.3100777700008));
#33297=CARTESIAN_POINT('Ctrl Pts',(-22.8280940049207,26.7078314963447,-18.2901283470691));
#33298=CARTESIAN_POINT('Ctrl Pts',(-23.1501613477646,26.7645688927759,-18.2728100441047));
#33299=CARTESIAN_POINT('Ctrl Pts',(-23.6306063543078,26.7757428592564,-18.2455409653934));
#33300=CARTESIAN_POINT('Ctrl Pts',(-23.7859310549281,26.7681230463719,-18.2365330128787));
#33301=CARTESIAN_POINT('Ctrl Pts',(-23.955229316461,26.7474925931426,-18.2262329649932));
#33302=CARTESIAN_POINT('Ctrl Pts',(-23.9703564997288,26.7455401322749,-18.2253085078733));
#33303=CARTESIAN_POINT('Ctrl Pts',(-23.9930608112159,26.7424456799021,-18.2239145797278));
#33304=CARTESIAN_POINT('Ctrl Pts',(-24.0006488010966,26.7413839089327,-18.2234476377551));
#33305=CARTESIAN_POINT('Ctrl Pts',(-24.0128659925645,26.7396299406051,-18.2226940643438));
#33306=CARTESIAN_POINT('Ctrl Pts',(-24.0174976296833,26.7389546953795,-18.222407969566));
#33307=CARTESIAN_POINT('Ctrl Pts',(-24.0263505382048,26.7376443295785,-18.2218603392672));
#33308=CARTESIAN_POINT('Ctrl Pts',(-24.0305720539617,26.7370109067949,-18.221598858062));
#33309=CARTESIAN_POINT('Ctrl Pts',(-24.0380618322143,26.7358718727354,-18.2211343262571));
#33310=CARTESIAN_POINT('Ctrl Pts',(-24.0413306046607,26.7353696136566,-18.2209313823916));
#33311=CARTESIAN_POINT('Ctrl Pts',(-24.0477816676953,26.7343682170087,-18.2205304515273));
#33312=CARTESIAN_POINT('Ctrl Pts',(-24.0509639951835,26.7338693379131,-18.2203324729523));
#33313=CARTESIAN_POINT('Ctrl Pts',(-24.0586248664506,26.7326566070337,-18.2198553957831));
#33314=CARTESIAN_POINT('Ctrl Pts',(-24.0631026530686,26.7319380727499,-18.219576148512));
#33315=CARTESIAN_POINT('Ctrl Pts',(-24.0768449981306,26.7297031239346,-18.2187179153245));
#33316=CARTESIAN_POINT('Ctrl Pts',(-24.0861043971485,26.7281556877863,-18.2181379431855));
#33317=CARTESIAN_POINT('Ctrl Pts',(-24.1202295320153,26.7222992926321,-18.2159940970215));
#33318=CARTESIAN_POINT('Ctrl Pts',(-24.1450506508554,26.7177388494945,-18.2144222331254));
#33319=CARTESIAN_POINT('Ctrl Pts',(-24.1757416351714,26.7117264625948,-18.212462655042));
#33320=CARTESIAN_POINT('Ctrl Pts',(-24.1816648674538,26.7105487987841,-18.2120837246081));
#33321=CARTESIAN_POINT('Ctrl Pts',(-24.1943149096219,26.7079967193742,-18.2112728658593));
#33322=CARTESIAN_POINT('Ctrl Pts',(-24.2010406985633,26.7066174444027,-18.2108407851845));
#33323=CARTESIAN_POINT('Ctrl Pts',(-24.2092195258783,26.7049129381032,-18.2103141802302));
#33324=CARTESIAN_POINT('Ctrl Pts',(-24.2106768521019,26.7046081705198,-18.2102203027552));
#33325=CARTESIAN_POINT('Ctrl Pts',(-24.2149499291643,26.7037114597849,-18.2099449076427));
#33326=CARTESIAN_POINT('Ctrl Pts',(-24.2177650936578,26.7031167566321,-18.2097633030979));
#33327=CARTESIAN_POINT('Ctrl Pts',(-24.2273194597711,26.7010850279332,-18.2091463774524));
#33328=CARTESIAN_POINT('Ctrl Pts',(-24.2340548124942,26.6996301660918,-18.2087104965281));
#33329=CARTESIAN_POINT('Ctrl Pts',(-24.2459811299407,26.6970139739804,-18.2079369378518));
#33330=CARTESIAN_POINT('Ctrl Pts',(-24.2511739992196,26.6958613682946,-18.2075995342262));
#33331=CARTESIAN_POINT('Ctrl Pts',(-24.2602719986079,26.6938183353587,-18.2070073661085));
#33332=CARTESIAN_POINT('Ctrl Pts',(-24.264178377251,26.6929334719395,-18.2067527751499));
#33333=CARTESIAN_POINT('Ctrl Pts',(-24.2723344098157,26.6910699955193,-18.2062205226688));
#33334=CARTESIAN_POINT('Ctrl Pts',(-24.2765837448691,26.6900900351729,-18.2059428199444));
#33335=CARTESIAN_POINT('Ctrl Pts',(-24.300816488232,26.6844497758177,-18.2043568947711));
#33336=CARTESIAN_POINT('Ctrl Pts',(-24.3207566627785,26.6796074127548,-18.203043097133));
#33337=CARTESIAN_POINT('Ctrl Pts',(-24.5746786807103,26.6153697946659,-18.1862000724388));
#33338=CARTESIAN_POINT('Ctrl Pts',(-24.8012843420482,26.5300641932563,-18.1698556441782));
#33339=CARTESIAN_POINT('Ctrl Pts',(-25.1804817650056,26.3363786438452,-18.1410641612364));
#33340=CARTESIAN_POINT('Ctrl Pts',(-25.3372774926578,26.238506057559,-18.1286851923449));
#33341=CARTESIAN_POINT('Ctrl Pts',(-25.4894785670449,26.124267566502,-18.1167655817952));
#33342=CARTESIAN_POINT('Ctrl Pts',(-25.4940950675145,26.1207830630774,-18.1164041559895));
#33343=CARTESIAN_POINT('Ctrl Pts',(-25.5007436745224,26.1157365860001,-18.1158838332921));
#33344=CARTESIAN_POINT('Ctrl Pts',(-25.5027833036801,26.1141846126407,-18.1157242379033));
#33345=CARTESIAN_POINT('Ctrl Pts',(-25.5063297218303,26.1114794230485,-18.1154467903434));
#33346=CARTESIAN_POINT('Ctrl Pts',(-25.5078373455214,26.1103273078513,-18.1153288599357));
#33347=CARTESIAN_POINT('Ctrl Pts',(-25.5107552607203,26.1080933733398,-18.115100644484));
#33348=CARTESIAN_POINT('Ctrl Pts',(-25.5121656711627,26.1070117215532,-18.1149903479462));
#33349=CARTESIAN_POINT('Ctrl Pts',(-25.5155323339002,26.1044253826419,-18.1147271011635));
#33350=CARTESIAN_POINT('Ctrl Pts',(-25.5174877575603,26.1029196113746,-18.1145742281793));
#33351=CARTESIAN_POINT('Ctrl Pts',(-25.524471524388,26.097528980691,-18.1140283295035));
#33352=CARTESIAN_POINT('Ctrl Pts',(-25.5294901482737,26.0936314648209,-18.1136361974022));
#33353=CARTESIAN_POINT('Ctrl Pts',(-25.6025391879921,26.0365536617826,-18.1079302485563));
#33354=CARTESIAN_POINT('Ctrl Pts',(-25.6684241479758,25.9806693583862,-18.1028061023772));
#33355=CARTESIAN_POINT('Ctrl Pts',(-25.8454757772924,25.8178157032674,-18.0888440465991));
#33356=CARTESIAN_POINT('Ctrl Pts',(-25.9513310879628,25.7054139877674,-18.0802618742853));
#33357=CARTESIAN_POINT('Ctrl Pts',(-26.144654827345,25.4681300964519,-18.0631590269419));
#33358=CARTESIAN_POINT('Ctrl Pts',(-26.2321269517698,25.3437750580544,-18.0546585686911));
#33359=CARTESIAN_POINT('Ctrl Pts',(-26.3499531767997,25.1482623858747,-18.0414607052276));
#33360=CARTESIAN_POINT('Ctrl Pts',(-26.3870603130505,25.0814218582283,-18.0369777477752));
#33361=CARTESIAN_POINT('Ctrl Pts',(-26.4416124099945,24.9743553693789,-18.0297985849056));
#33362=CARTESIAN_POINT('Ctrl Pts',(-26.4606738134305,24.9349830161767,-18.0271590784457));
#33363=CARTESIAN_POINT('Ctrl Pts',(-26.4821224871873,24.8882789666404,-18.0240244761523));
#33364=CARTESIAN_POINT('Ctrl Pts',(-26.4852928131585,24.8813102769195,-18.0235566739027));
#33365=CARTESIAN_POINT('Ctrl Pts',(-26.4901085988584,24.8706238414046,-18.0228391415516));
#33366=CARTESIAN_POINT('Ctrl Pts',(-26.491771920128,24.8669141352873,-18.0225900266542));
#33367=CARTESIAN_POINT('Ctrl Pts',(-26.4947904090256,24.8601477303123,-18.0221355898311));
#33368=CARTESIAN_POINT('Ctrl Pts',(-26.4961478496797,24.8570920466073,-18.0219303463571));
#33369=CARTESIAN_POINT('Ctrl Pts',(-26.4988657972233,24.8509480232269,-18.0215176204885));
#33370=CARTESIAN_POINT('Ctrl Pts',(-26.5002262133418,24.847859648196,-18.0213101352958));
#33371=CARTESIAN_POINT('Ctrl Pts',(-26.5040792661313,24.8390751898206,-18.0207199033599));
#33372=CARTESIAN_POINT('Ctrl Pts',(-26.506560263094,24.8333740448697,-18.0203367585644));
#33373=CARTESIAN_POINT('Ctrl Pts',(-26.5169876633755,24.8092218749029,-18.0187132379315));
#33374=CARTESIAN_POINT('Ctrl Pts',(-26.5247778118972,24.7907042545325,-18.0174675419625));
#33375=CARTESIAN_POINT('Ctrl Pts',(-26.6616749743222,24.4565859505783,-17.9949707901166));
#33376=CARTESIAN_POINT('Ctrl Pts',(-26.740031370464,24.1225972304051,-17.9718102504194));
#33377=CARTESIAN_POINT('Ctrl Pts',(-26.7702366830597,23.7048670766068,-17.9435926650705));
#33378=CARTESIAN_POINT('Ctrl Pts',(-26.77303610225,23.6268743742366,-17.9383726663722));
#33379=CARTESIAN_POINT('Ctrl Pts',(-26.7729984130383,23.540066620556,-17.93266390827));
#33380=CARTESIAN_POINT('Ctrl Pts',(-26.7729586632714,23.5312798995657,-17.932087226881));
#33381=CARTESIAN_POINT('Ctrl Pts',(-26.7728346119646,23.5168784717514,-17.9311440606414));
#33382=CARTESIAN_POINT('Ctrl Pts',(-26.7727715714455,23.5112636722634,-17.9307768427314));
#33383=CARTESIAN_POINT('Ctrl Pts',(-26.7726105908347,23.4996334059842,-17.9300172787948));
#33384=CARTESIAN_POINT('Ctrl Pts',(-26.7725104801115,23.4936179836301,-17.9296250125336));
#33385=CARTESIAN_POINT('Ctrl Pts',(-26.7723805932278,23.486937761939,-17.9291900815134));
#33386=CARTESIAN_POINT('Ctrl Pts',(-26.7723674558826,23.4862726886051,-17.9291467879639));
#33387=CARTESIAN_POINT('Ctrl Pts',(-26.7722800001526,23.4819136256339,-17.9288630805769));
#33388=CARTESIAN_POINT('Ctrl Pts',(-26.7721995349435,23.4782197470498,-17.9286229005753));
#33389=CARTESIAN_POINT('Ctrl Pts',(-26.7708675209552,23.4215478951566,-17.924941707468));
#33390=CARTESIAN_POINT('Ctrl Pts',(-26.7683157127863,23.3686045912169,-17.9215518572488));
#33391=CARTESIAN_POINT('Ctrl Pts',(-26.7640404577051,23.310007193485,-17.917872014338));
#33392=CARTESIAN_POINT('Ctrl Pts',(-26.7636064901182,23.3042708352119,-17.9175125458878));
#33393=CARTESIAN_POINT('Ctrl Pts',(-26.762977359392,23.2962406357882,-17.9170104382764));
#33394=CARTESIAN_POINT('Ctrl Pts',(-26.7627950981227,23.2939458389715,-17.9168670768707));
#33395=CARTESIAN_POINT('Ctrl Pts',(-26.7624572316607,23.2897488454673,-17.9166051142168));
#33396=CARTESIAN_POINT('Ctrl Pts',(-26.7623023953219,23.2878465892089,-17.9164864693392));
#33397=CARTESIAN_POINT('Ctrl Pts',(-26.761984594664,23.2839846495293,-17.916245777536));
#33398=CARTESIAN_POINT('Ctrl Pts',(-26.7618215264956,23.2820249770673,-17.9161237366613));
#33399=CARTESIAN_POINT('Ctrl Pts',(-26.7614120981776,23.2771585719892,-17.915820906119));
#33400=CARTESIAN_POINT('Ctrl Pts',(-26.7611635842041,23.2742520148904,-17.9156402388072));
#33401=CARTESIAN_POINT('Ctrl Pts',(-26.7602215564562,23.2634077828197,-17.9149669261762));
#33402=CARTESIAN_POINT('Ctrl Pts',(-26.7595025449506,23.2554722652478,-17.9144757115415));
#33403=CARTESIAN_POINT('Ctrl Pts',(-26.7468016128444,23.1208531956469,-17.9061668717925));
#33404=CARTESIAN_POINT('Ctrl Pts',(-26.7273546650133,22.9949683280943,-17.8987592711115));
#33405=CARTESIAN_POINT('Ctrl Pts',(-26.624848631325,22.5198786645754,-17.8710877456227));
#33406=CARTESIAN_POINT('Ctrl Pts',(-26.4911833219502,22.1843281864495,-17.8518211454671));
#33407=CARTESIAN_POINT('Ctrl Pts',(-26.3004775288236,21.8702359567385,-17.8296770502588));
#33408=CARTESIAN_POINT('Ctrl Pts',(-26.2959330104918,21.8628189972855,-17.829151775918));
#33409=CARTESIAN_POINT('Ctrl Pts',(-26.281189611876,21.8389740262555,-17.8274553279706));
#33410=CARTESIAN_POINT('Ctrl Pts',(-26.2708730349854,21.8226196103841,-17.8262799098585));
#33411=CARTESIAN_POINT('Ctrl Pts',(-26.2570960450433,21.8012090030495,-17.8247249961102));
#33412=CARTESIAN_POINT('Ctrl Pts',(-26.2537673524116,21.7960681958284,-17.8243504191986));
#33413=CARTESIAN_POINT('Ctrl Pts',(-26.2485920153734,21.7881251652126,-17.8237697378153));
#33414=CARTESIAN_POINT('Ctrl Pts',(-26.2467556011114,21.7853162661671,-17.8235640170239));
#33415=CARTESIAN_POINT('Ctrl Pts',(-26.2432633238885,21.7799928048318,-17.8231734196512));
#33416=CARTESIAN_POINT('Ctrl Pts',(-26.2416083169426,21.7774776828937,-17.8229885753775));
#33417=CARTESIAN_POINT('Ctrl Pts',(-26.2377722925888,21.7716658110838,-17.8225607398063));
#33418=CARTESIAN_POINT('Ctrl Pts',(-26.2355887327341,21.768370752481,-17.822317652915));
#33419=CARTESIAN_POINT('Ctrl Pts',(-26.2294474433035,21.7591402848179,-17.8216352148396));
#33420=CARTESIAN_POINT('Ctrl Pts',(-26.2254760779039,21.753214014634,-17.8211953489767));
#33421=CARTESIAN_POINT('Ctrl Pts',(-26.2023311417576,21.7189227391416,-17.8186401020144));
#33422=CARTESIAN_POINT('Ctrl Pts',(-26.182726811209,21.6908524174493,-17.8165083994494));
#33423=CARTESIAN_POINT('Ctrl Pts',(-26.124822155427,21.6106936942847,-17.8103016261583));
#33424=CARTESIAN_POINT('Ctrl Pts',(-26.0853987012908,21.5594410967762,-17.8061836435481));
#33425=CARTESIAN_POINT('Ctrl Pts',(-25.9941686199034,21.4479444134286,-17.7968809963556));
#33426=CARTESIAN_POINT('Ctrl Pts',(-25.9416227292213,21.3883616194807,-17.791670534089));
#33427=CARTESIAN_POINT('Ctrl Pts',(-25.6939991327186,21.1276608468566,-17.7677933779304));
#33428=CARTESIAN_POINT('Ctrl Pts',(-25.4754210128618,20.9505766118356,-17.7483776422649));
#33429=CARTESIAN_POINT('Ctrl Pts',(-25.2309597035605,20.8004549906187,-17.7297135635187));
#33430=CARTESIAN_POINT('Ctrl Pts',(-25.2251972307697,20.7969411851593,-17.7292752696607));
#33431=CARTESIAN_POINT('Ctrl Pts',(-25.1768645579165,20.7676770751543,-17.7256132031939));
#33432=CARTESIAN_POINT('Ctrl Pts',(-25.1337113701679,20.7428958306231,-17.7224349727554));
#33433=CARTESIAN_POINT('Ctrl Pts',(-25.0850936303776,20.7164544546487,-17.7189691218883));
#33434=CARTESIAN_POINT('Ctrl Pts',(-25.0801815192066,20.7137994589362,-17.7186202327174));
#33435=CARTESIAN_POINT('Ctrl Pts',(-25.0732261236062,20.7100633929081,-17.7181280570423));
#33436=CARTESIAN_POINT('Ctrl Pts',(-25.0711885741907,20.7089717535138,-17.7179840993204));
#33437=CARTESIAN_POINT('Ctrl Pts',(-25.0674643593718,20.7069816187229,-17.717721383831));
#33438=CARTESIAN_POINT('Ctrl Pts',(-25.0657780672334,20.7060824302802,-17.7176025815439));
#33439=CARTESIAN_POINT('Ctrl Pts',(-25.0623578205465,20.7042625436278,-17.7173619306523));
#33440=CARTESIAN_POINT('Ctrl Pts',(-25.0606238236938,20.703341929462,-17.7172400875017));
#33441=CARTESIAN_POINT('Ctrl Pts',(-25.0563768262911,20.7010920845256,-17.7169420566286));
#33442=CARTESIAN_POINT('Ctrl Pts',(-25.0538629000821,20.6997645901814,-17.7167659803341));
#33443=CARTESIAN_POINT('Ctrl Pts',(-25.044699539618,20.6949413160418,-17.7161253906069));
#33444=CARTESIAN_POINT('Ctrl Pts',(-25.0380395770449,20.6914654273294,-17.7156621359239));
#33445=CARTESIAN_POINT('Ctrl Pts',(-24.8896497576756,20.6146785764687,-17.7053907428935));
#33446=CARTESIAN_POINT('Ctrl Pts',(-24.7426582163145,20.5519590711582,-17.6962308940142));
#33447=CARTESIAN_POINT('Ctrl Pts',(-24.3366523796988,20.4133318871669,-17.6720439822094));
#33448=CARTESIAN_POINT('Ctrl Pts',(-24.0718103769255,20.3585963144676,-17.6573243651315));
#33449=CARTESIAN_POINT('Ctrl Pts',(-23.7931436461296,20.3366526583845,-17.6409112173878));
#33450=CARTESIAN_POINT('Ctrl Pts',(-23.7830383483094,20.3359048529803,-17.6403149457771));
#33451=CARTESIAN_POINT('Ctrl Pts',(-23.7037038974258,20.3304100742564,-17.6356247778303));
#33452=CARTESIAN_POINT('Ctrl Pts',(-23.6343456308052,20.3278528016023,-17.631470210821));
#33453=CARTESIAN_POINT('Ctrl Pts',(-23.5564528463312,20.3274972608486,-17.6267258576395));
#33454=CARTESIAN_POINT('Ctrl Pts',(-23.5479430519864,20.3274921242511,-17.6262064931044));
#33455=CARTESIAN_POINT('Ctrl Pts',(-23.5351179497119,20.3275351797913,-17.6254221537604));
#33456=CARTESIAN_POINT('Ctrl Pts',(-23.5308025488109,20.3275583352649,-17.6251579646609));
#33457=CARTESIAN_POINT('Ctrl Pts',(-23.5233242313344,20.3276134836149,-17.624699662203));
#33458=CARTESIAN_POINT('Ctrl Pts',(-23.5201612832678,20.3276414654583,-17.6245056749394));
#33459=CARTESIAN_POINT('Ctrl Pts',(-23.5135899992366,20.3277092752619,-17.6241023395748));
#33460=CARTESIAN_POINT('Ctrl Pts',(-23.5101816768893,20.3277498540663,-17.6238929681766));
#33461=CARTESIAN_POINT('Ctrl Pts',(-23.5021733516143,20.3278579066417,-17.6234006098322));
#33462=CARTESIAN_POINT('Ctrl Pts',(-23.4975734250476,20.3279298230729,-17.6231174837589));
#33463=CARTESIAN_POINT('Ctrl Pts',(-23.4828573222579,20.3281914178381,-17.6222106762619));
#33464=CARTESIAN_POINT('Ctrl Pts',(-23.4727419542397,20.3284188857227,-17.6215858096862));
#33465=CARTESIAN_POINT('Ctrl Pts',(-23.2491595853086,20.3345002027843,-17.6077391870997));
#33466=CARTESIAN_POINT('Ctrl Pts',(-23.0368413899666,20.3615072999008,-17.5938286696543));
#33467=CARTESIAN_POINT('Ctrl Pts',(-22.5856794462837,20.465137172929,-17.5627797848461));
#33468=CARTESIAN_POINT('Ctrl Pts',(-22.3498759310134,20.5490129724615,-17.5455846795741));
#33469=CARTESIAN_POINT('Ctrl Pts',(-22.1251251987002,20.6597282129364,-17.5293710257841));
#33470=CARTESIAN_POINT('Ctrl Pts',(-22.1241468316802,20.6602107871911,-17.5293004507838));
#33471=CARTESIAN_POINT('Ctrl Pts',(-22.1204316023287,20.6620456499874,-17.5290324702955));
#33472=CARTESIAN_POINT('Ctrl Pts',(-22.1176964077432,20.6634013347216,-17.5288352201083));
#33473=CARTESIAN_POINT('Ctrl Pts',(-22.1136045082945,20.6654367105488,-17.5285401948741));
#33474=CARTESIAN_POINT('Ctrl Pts',(-22.1122463582643,20.6661134729342,-17.5284422831528));
#33475=CARTESIAN_POINT('Ctrl Pts',(-22.1085530970545,20.6679570720138,-17.52817605864));
#33476=CARTESIAN_POINT('Ctrl Pts',(-22.1062189195616,20.6691257896266,-17.5280078347616));
#33477=CARTESIAN_POINT('Ctrl Pts',(-22.0686854646964,20.6879757798333,-17.5253033586762));
#33478=CARTESIAN_POINT('Ctrl Pts',(-22.0338098159976,20.7062991179851,-17.5227982288467));
#33479=CARTESIAN_POINT('Ctrl Pts',(-21.9950911342815,20.7275564103991,-17.5200332547236));
#33480=CARTESIAN_POINT('Ctrl Pts',(-21.9909103631002,20.7298638409071,-17.5197349127339));
#33481=CARTESIAN_POINT('Ctrl Pts',(-21.9846263647103,20.7333503180641,-17.5192868249005));
#33482=CARTESIAN_POINT('Ctrl Pts',(-21.9825193302346,20.7345224336497,-17.5191366382788));
#33483=CARTESIAN_POINT('Ctrl Pts',(-21.9788743474002,20.7365554494167,-17.5188769317378));
#33484=CARTESIAN_POINT('Ctrl Pts',(-21.9773357901874,20.7374152464581,-17.5187673407121));
#33485=CARTESIAN_POINT('Ctrl Pts',(-21.9741335248613,20.7392082279637,-17.5185393117267));
#33486=CARTESIAN_POINT('Ctrl Pts',(-21.9724699417812,20.7401416263702,-17.5184208884038));
#33487=CARTESIAN_POINT('Ctrl Pts',(-21.9685682311875,20.7423353438793,-17.518143229893));
#33488=CARTESIAN_POINT('Ctrl Pts',(-21.9663307735301,20.7435968662767,-17.5179840726572));
#33489=CARTESIAN_POINT('Ctrl Pts',(-21.9589987694759,20.7477423536151,-17.517462738449));
#33490=CARTESIAN_POINT('Ctrl Pts',(-21.9539105347606,20.7506375467164,-17.517101283876));
#33491=CARTESIAN_POINT('Ctrl Pts',(-21.941921902915,20.7575023597134,-17.516250376214));
#33492=CARTESIAN_POINT('Ctrl Pts',(-21.9350282322035,20.7614837352554,-17.515761664554));
#33493=CARTESIAN_POINT('Ctrl Pts',(-21.6937703901942,20.9020146471463,-17.4986758783388));
#33494=CARTESIAN_POINT('Ctrl Pts',(-21.4775192327476,21.0676083704097,-17.4838872958859));
#33495=CARTESIAN_POINT('Ctrl Pts',(-21.1775862598352,21.3641154601481,-17.4602493636112));
#33496=CARTESIAN_POINT('Ctrl Pts',(-21.078163242266,21.4772091025496,-17.4517329920023));
#33497=CARTESIAN_POINT('Ctrl Pts',(-20.9784172347789,21.6080935329503,-17.4420773547995));
#33498=CARTESIAN_POINT('Ctrl Pts',(-20.9699023745134,21.6194207346154,-17.4412433658083));
#33499=CARTESIAN_POINT('Ctrl Pts',(-20.9569341314748,21.6369112011389,-17.4399578454422));
#33500=CARTESIAN_POINT('Ctrl Pts',(-20.9524273320497,21.6430347667681,-17.4395081935723));
#33501=CARTESIAN_POINT('Ctrl Pts',(-20.9455429478767,21.6524585254603,-17.4388168143472));
#33502=CARTESIAN_POINT('Ctrl Pts',(-20.9431498521397,21.6557473920403,-17.4385756373674));
#33503=CARTESIAN_POINT('Ctrl Pts',(-20.9372203180953,21.6639289491493,-17.4379759428479));
#33504=CARTESIAN_POINT('Ctrl Pts',(-20.9336913988822,21.6688270495339,-17.43761715932));
#33505=CARTESIAN_POINT('Ctrl Pts',(-20.9261380232371,21.6793734046566,-17.4368451313633));
#33506=CARTESIAN_POINT('Ctrl Pts',(-20.922118000637,21.6850247849946,-17.4364317305295));
#33507=CARTESIAN_POINT('Ctrl Pts',(-20.9143089420797,21.6960781889489,-17.4356237178964));
#33508=CARTESIAN_POINT('Ctrl Pts',(-20.9105181908848,21.7014789625608,-17.4352291708948));
#33509=CARTESIAN_POINT('Ctrl Pts',(-20.9039556380263,21.7108901207165,-17.4345420660109));
#33510=CARTESIAN_POINT('Ctrl Pts',(-20.9011762914153,21.7148952364636,-17.4342497844195));
#33511=CARTESIAN_POINT('Ctrl Pts',(-20.8916725354774,21.7286569740134,-17.43324592072));
#33512=CARTESIAN_POINT('Ctrl Pts',(-20.8849929121193,21.7384442839333,-17.4325327102821));
#33513=CARTESIAN_POINT('Ctrl Pts',(-20.8756716281177,21.7522653797618,-17.4315264790985));
#33514=CARTESIAN_POINT('Ctrl Pts',(-20.8729847576868,21.7562686760909,-17.4312351315986));
#33515=CARTESIAN_POINT('Ctrl Pts',(-20.8593407233764,21.7766964916836,-17.4297489865336));
#33516=CARTESIAN_POINT('Ctrl Pts',(-20.848525862262,21.7932151490841,-17.4285489684857));
#33517=CARTESIAN_POINT('Ctrl Pts',(-20.8345287765827,21.8150291507777,-17.4269661365636));
#33518=CARTESIAN_POINT('Ctrl Pts',(-20.8312088649958,21.8202359902979,-17.4265884654841));
#33519=CARTESIAN_POINT('Ctrl Pts',(-20.8261023883533,21.8282958277458,-17.4260040581387));
#33520=CARTESIAN_POINT('Ctrl Pts',(-20.8243052812225,21.8311421567484,-17.4257977136756));
#33521=CARTESIAN_POINT('Ctrl Pts',(-20.8207316250555,21.8368219473462,-17.4253860323648));
#33522=CARTESIAN_POINT('Ctrl Pts',(-20.818955020483,21.8396553692171,-17.4251806979121));
#33523=CARTESIAN_POINT('Ctrl Pts',(-20.8150209574246,21.845951372347,-17.4247245140569));
#33524=CARTESIAN_POINT('Ctrl Pts',(-20.8128656596926,21.8494152909852,-17.4244735851987));
#33525=CARTESIAN_POINT('Ctrl Pts',(-20.8066495575367,21.8594480125048,-17.42374695506));
#33526=CARTESIAN_POINT('Ctrl Pts',(-20.8026058003689,21.8660272973236,-17.4232706262943));
#33527=CARTESIAN_POINT('Ctrl Pts',(-20.7786683636123,21.9052897029333,-17.4204291035387));
#33528=CARTESIAN_POINT('Ctrl Pts',(-20.7593350587508,21.9383093055352,-17.4180434764323));
#33529=CARTESIAN_POINT('Ctrl Pts',(-20.70332229656,22.0380038755256,-17.4108491971482));
#33530=CARTESIAN_POINT('Ctrl Pts',(-20.6684137181855,22.1056379574815,-17.4059790169273));
#33531=CARTESIAN_POINT('Ctrl Pts',(-20.5290299739496,22.4008879412209,-17.3847574894445));
#33532=CARTESIAN_POINT('Ctrl Pts',(-20.4488944814781,22.6390052990426,-17.3676497595669));
#33533=CARTESIAN_POINT('Ctrl Pts',(-20.367363341557,23.024830474815,-17.3411145481398));
#33534=CARTESIAN_POINT('Ctrl Pts',(-20.3470638832927,23.1675705633021,-17.3315638048573));
#33535=CARTESIAN_POINT('Ctrl Pts',(-20.3356944587533,23.3204276908054,-17.3219255173698));
#33536=CARTESIAN_POINT('Ctrl Pts',(-20.3350482762301,23.3296518462194,-17.3213461888227));
#33537=CARTESIAN_POINT('Ctrl Pts',(-20.3342315252711,23.3420777817474,-17.3205689744489));
#33538=CARTESIAN_POINT('Ctrl Pts',(-20.3340260293567,23.3452771035423,-17.3203691499387));
#33539=CARTESIAN_POINT('Ctrl Pts',(-20.3337109223972,23.3503000976843,-17.3200558762167));
#33540=CARTESIAN_POINT('Ctrl Pts',(-20.3335980882279,23.3521235545747,-17.3199422449907));
#33541=CARTESIAN_POINT('Ctrl Pts',(-20.3333839677419,23.3556322475165,-17.3197237781004));
#33542=CARTESIAN_POINT('Ctrl Pts',(-20.3332824557748,23.3573174560571,-17.3196189305044));
#33543=CARTESIAN_POINT('Ctrl Pts',(-20.3330446243956,23.3613180895402,-17.3193702169233));
#33544=CARTESIAN_POINT('Ctrl Pts',(-20.3329094804741,23.3636335801801,-17.3192264182362));
#33545=CARTESIAN_POINT('Ctrl Pts',(-20.3325228812875,23.3703826369332,-17.3188077200045));
#33546=CARTESIAN_POINT('Ctrl Pts',(-20.3322780884589,23.3748166020971,-17.3185331960443));
#33547=CARTESIAN_POINT('Ctrl Pts',(-20.3305228783936,23.4078492752377,-17.3164920219037));
#33548=CARTESIAN_POINT('Ctrl Pts',(-20.329384502001,23.4364676448994,-17.3147459860348));
#33549=CARTESIAN_POINT('Ctrl Pts',(-20.3268609144045,23.5319423870339,-17.3089842438403));
#33550=CARTESIAN_POINT('Ctrl Pts',(-20.3271747612635,23.5988299816057,-17.3050509569519));
#33551=CARTESIAN_POINT('Ctrl Pts',(-20.3362243331168,23.85136817129,-17.2904304812832));
#33552=CARTESIAN_POINT('Ctrl Pts',(-20.3589282845446,24.0361607395012,-17.2801853618862));
#33553=CARTESIAN_POINT('Ctrl Pts',(-20.4286585349257,24.3654087878855,-17.2613224123456));
#33554=CARTESIAN_POINT('Ctrl Pts',(-20.4701832453469,24.5104587224931,-17.2527888340894));
#33555=CARTESIAN_POINT('Ctrl Pts',(-20.5261481902739,24.6642901584963,-17.2431821416407));
#33556=CARTESIAN_POINT('Ctrl Pts',(-20.530671131705,24.676491877446,-17.2424163273379));
#33557=CARTESIAN_POINT('Ctrl Pts',(-20.5411591738803,24.7042685111507,-17.2406639440555));
#33558=CARTESIAN_POINT('Ctrl Pts',(-20.5471714934166,24.7198250945627,-17.2396759778056));
#33559=CARTESIAN_POINT('Ctrl Pts',(-20.555848407541,24.7417681098752,-17.2382727989229));
#33560=CARTESIAN_POINT('Ctrl Pts',(-20.558413299277,24.748193865019,-17.2378607204718));
#33561=CARTESIAN_POINT('Ctrl Pts',(-20.5618042222262,24.7566102351161,-17.2373194215051));
#33562=CARTESIAN_POINT('Ctrl Pts',(-20.5626115989688,24.7586083832702,-17.2371907947248));
#33563=CARTESIAN_POINT('Ctrl Pts',(-20.5648144138758,24.7640443478743,-17.2368405486044));
#33564=CARTESIAN_POINT('Ctrl Pts',(-20.5662137826276,24.7674805597356,-17.2366188039469));
#33565=CARTESIAN_POINT('Ctrl Pts',(-20.5687829468273,24.7737581995025,-17.2362130610085));
#33566=CARTESIAN_POINT('Ctrl Pts',(-20.5699508795061,24.7766003887535,-17.2360291228707));
#33567=CARTESIAN_POINT('Ctrl Pts',(-20.5734397759833,24.7850562733642,-17.2354811673729));
#33568=CARTESIAN_POINT('Ctrl Pts',(-20.5757725397995,24.7906650598765,-17.2351167687178));
#33569=CARTESIAN_POINT('Ctrl Pts',(-20.583218490467,24.808425961502,-17.233959839686));
#33570=CARTESIAN_POINT('Ctrl Pts',(-20.5883903498938,24.82055320062,-17.2331653943517));
#33571=CARTESIAN_POINT('Ctrl Pts',(-20.6020491859439,24.8520442098543,-17.2310904677951));
#33572=CARTESIAN_POINT('Ctrl Pts',(-20.610652450546,24.8713565665989,-17.2298061221463));
#33573=CARTESIAN_POINT('Ctrl Pts',(-20.6220830521878,24.8963510784387,-17.2281279285943));
#33574=CARTESIAN_POINT('Ctrl Pts',(-20.6247381621318,24.9021117961281,-17.2277400297952));
#33575=CARTESIAN_POINT('Ctrl Pts',(-20.6290016776327,24.9112908419168,-17.2271201701073));
#33576=CARTESIAN_POINT('Ctrl Pts',(-20.6305991259422,24.9147142659822,-17.2268885888975));
#33577=CARTESIAN_POINT('Ctrl Pts',(-20.6334838144629,24.9208680593313,-17.2264715894135));
#33578=CARTESIAN_POINT('Ctrl Pts',(-20.6347688802546,24.9235994479928,-17.226286246774));
#33579=CARTESIAN_POINT('Ctrl Pts',(-20.6377868515448,24.9299907759293,-17.2258519524374));
#33580=CARTESIAN_POINT('Ctrl Pts',(-20.6395228187341,24.9336492566099,-17.2256028945295));
#33581=CARTESIAN_POINT('Ctrl Pts',(-20.6445283297067,24.944147036498,-17.2248869044704));
#33582=CARTESIAN_POINT('Ctrl Pts',(-20.6478150992536,24.9509780500352,-17.2244193729758));
#33583=CARTESIAN_POINT('Ctrl Pts',(-20.6691922366224,24.9950086391638,-17.2213951919681));
#33584=CARTESIAN_POINT('Ctrl Pts',(-20.687972588244,25.0318671583642,-17.2188144875263));
#33585=CARTESIAN_POINT('Ctrl Pts',(-20.7362097283019,25.1221960822656,-17.2123635671191));
#33586=CARTESIAN_POINT('Ctrl Pts',(-20.7664852211094,25.1752085873638,-17.2084650994785));
#33587=CARTESIAN_POINT('Ctrl Pts',(-20.8659280990381,25.338390056095,-17.1961040905956));
#33588=CARTESIAN_POINT('Ctrl Pts',(-20.9402645650632,25.4452433490221,-17.1874717513421));
#33589=CARTESIAN_POINT('Ctrl Pts',(-21.1034615225553,25.651943766477,-17.1697564257296));
#33590=CARTESIAN_POINT('Ctrl Pts',(-21.1924896728254,25.7513536056379,-17.1606844528849));
#33591=CARTESIAN_POINT('Ctrl Pts',(-21.3892756791728,25.9454060623534,-17.1420912907719));
#33592=CARTESIAN_POINT('Ctrl Pts',(-21.4977228114358,26.0389698830556,-17.1326063673031));
#33593=CARTESIAN_POINT('Ctrl Pts',(-21.6193935505197,26.1305598413619,-17.1230306726729));
#33594=CARTESIAN_POINT('Ctrl Pts',(-21.6267681916344,26.1360619245084,-17.1224542279697));
#33595=CARTESIAN_POINT('Ctrl Pts',(-21.6367395298454,26.1434350928297,-17.1216802348175));
#33596=CARTESIAN_POINT('Ctrl Pts',(-21.6393155042683,26.1453339333167,-17.1214807683727));
#33597=CARTESIAN_POINT('Ctrl Pts',(-21.6433655873451,26.1483100902344,-17.1211679237028));
#33598=CARTESIAN_POINT('Ctrl Pts',(-21.6448377815073,26.1493899897421,-17.121054364309));
#33599=CARTESIAN_POINT('Ctrl Pts',(-21.6476732924421,26.1514662199852,-17.1208359506526));
#33600=CARTESIAN_POINT('Ctrl Pts',(-21.6490364655166,26.1524627237249,-17.120731084598));
#33601=CARTESIAN_POINT('Ctrl Pts',(-21.6522759710349,26.1548269554595,-17.1204821990784));
#33602=CARTESIAN_POINT('Ctrl Pts',(-21.6541529970658,26.1561937260822,-17.120338247187));
#33603=CARTESIAN_POINT('Ctrl Pts',(-21.6596336762357,26.1601754673729,-17.1199186689952));
#33604=CARTESIAN_POINT('Ctrl Pts',(-21.6632412919604,26.1627850134982,-17.1196434207054));
#33605=CARTESIAN_POINT('Ctrl Pts',(-21.6903411039546,26.1823020731279,-17.1175827151332));
#33606=CARTESIAN_POINT('Ctrl Pts',(-21.7140556801442,26.1989005965808,-17.1158183212167));
#33607=CARTESIAN_POINT('Ctrl Pts',(-21.7944481134526,26.2535708153226,-17.1099547007653));
#33608=CARTESIAN_POINT('Ctrl Pts',(-21.8521146139147,26.2901627286824,-17.1059416532585));
#33609=CARTESIAN_POINT('Ctrl Pts',(-21.9647388341749,26.3567046957881,-17.0983797782872));
#33610=CARTESIAN_POINT('Ctrl Pts',(-22.0194731270377,26.3869297398572,-17.0948230931305));
#33611=CARTESIAN_POINT('Ctrl Pts',(-22.0750360832114,26.4155368094973,-17.0912958973716));
#33612=CARTESIAN_POINT('Origin',(-23.5502525316942,23.5502525316942,-77.3107734492734));
#33613=CARTESIAN_POINT('',(-22.0750358970872,26.4155367136697,-15.5960174792939));
#33614=CARTESIAN_POINT('',(-22.0750360164986,26.4155367751497,-15.845717117064));
#33615=CARTESIAN_POINT('',(-22.0750360153461,26.4155367745563,-77.3107734492734));
#33616=CARTESIAN_POINT('Ctrl Pts',(-22.0750358970872,26.4155367136697,-15.5960174792939));
#33617=CARTESIAN_POINT('Ctrl Pts',(-22.010768538295,26.382448101605,-15.6000629323526));
#33618=CARTESIAN_POINT('Ctrl Pts',(-21.9476108572898,26.3471954248686,-15.6041236814064));
#33619=CARTESIAN_POINT('Ctrl Pts',(-21.7815274076261,26.2470138169797,-15.6151340211213));
#33620=CARTESIAN_POINT('Ctrl Pts',(-21.681032103164,26.1783546106423,-15.6221567777815));
#33621=CARTESIAN_POINT('Ctrl Pts',(-21.5573531351805,26.0831672900697,-15.6314417263071));
#33622=CARTESIAN_POINT('Ctrl Pts',(-21.5303829102972,26.0617126157181,-15.6335079648564));
#33623=CARTESIAN_POINT('Ctrl Pts',(-21.4873738060228,26.0263581465605,-15.6368739757199));
#33624=CARTESIAN_POINT('Ctrl Pts',(-21.4711186838194,26.0127248791463,-15.6381630142914));
#33625=CARTESIAN_POINT('Ctrl Pts',(-21.450343128026,25.9949479355673,-15.6398329156864));
#33626=CARTESIAN_POINT('Ctrl Pts',(-21.4456980090794,25.9909502560865,-15.6402077434834));
#33627=CARTESIAN_POINT('Ctrl Pts',(-21.438244431871,25.9844984639567,-15.6408115631217));
#33628=CARTESIAN_POINT('Ctrl Pts',(-21.4354287659736,25.9820526699072,-15.6410402091086));
#33629=CARTESIAN_POINT('Ctrl Pts',(-21.430082699872,25.9773925673824,-15.6414753807729));
#33630=CARTESIAN_POINT('Ctrl Pts',(-21.4275515054041,25.9751791741847,-15.6416818681135));
#33631=CARTESIAN_POINT('Ctrl Pts',(-21.4218007934832,25.9701345828742,-15.64215201569));
#33632=CARTESIAN_POINT('Ctrl Pts',(-21.4185834572788,25.9673009177249,-15.6424157789755));
#33633=CARTESIAN_POINT('Ctrl Pts',(-21.4088329865162,25.9586785913056,-15.6432173713615));
#33634=CARTESIAN_POINT('Ctrl Pts',(-21.4023177464113,25.9528698355637,-15.6437560441706));
#33635=CARTESIAN_POINT('Ctrl Pts',(-21.3565091238014,25.9116932525387,-15.6475651877568));
#33636=CARTESIAN_POINT('Ctrl Pts',(-21.318069610961,25.8753915145602,-15.6508751805944));
#33637=CARTESIAN_POINT('Ctrl Pts',(-21.2781649337681,25.8358042641474,-15.6544377548644));
#33638=CARTESIAN_POINT('Ctrl Pts',(-21.2757914964577,25.833442355915,-15.6546501362696));
#33639=CARTESIAN_POINT('Ctrl Pts',(-21.270526431938,25.8281865098886,-15.6551223542594));
#33640=CARTESIAN_POINT('Ctrl Pts',(-21.2676366290336,25.825290759856,-15.6553822685019));
#33641=CARTESIAN_POINT('Ctrl Pts',(-21.2611691643497,25.8187852579012,-15.6559656075945));
#33642=CARTESIAN_POINT('Ctrl Pts',(-21.2575945177382,25.8151725353809,-15.6562891594675));
#33643=CARTESIAN_POINT('Ctrl Pts',(-21.2401038824574,25.797411761369,-15.6578778644677));
#33644=CARTESIAN_POINT('Ctrl Pts',(-21.2263104660075,25.7831440724978,-15.6591481228983));
#33645=CARTESIAN_POINT('Ctrl Pts',(-21.1736817696435,25.7276898874861,-15.6640624482381));
#33646=CARTESIAN_POINT('Ctrl Pts',(-21.1358041340041,25.6856120726269,-15.6677439030843));
#33647=CARTESIAN_POINT('Ctrl Pts',(-21.0300368851294,25.5617028156594,-15.6784466643746));
#33648=CARTESIAN_POINT('Ctrl Pts',(-20.9650655598877,25.4774849240265,-15.685557778967));
#33649=CARTESIAN_POINT('Ctrl Pts',(-20.801508943067,25.2422899061871,-15.7048807677061));
#33650=CARTESIAN_POINT('Ctrl Pts',(-20.7112242492433,25.0859946485086,-15.7171836028927));
#33651=CARTESIAN_POINT('Ctrl Pts',(-20.6096552457239,24.8702526005743,-15.7329056498722));
#33652=CARTESIAN_POINT('Ctrl Pts',(-20.5862692555078,24.8168687464365,-15.7366984038022));
#33653=CARTESIAN_POINT('Ctrl Pts',(-20.55405410004,24.7375436213785,-15.7421629942875));
#33654=CARTESIAN_POINT('Ctrl Pts',(-20.5440883340895,24.7120795896661,-15.7438917807212));
#33655=CARTESIAN_POINT('Ctrl Pts',(-20.5329002022171,24.6823840354266,-15.7458759685245));
#33656=CARTESIAN_POINT('Ctrl Pts',(-20.531361316529,24.6782740977499,-15.7461498806865));
#33657=CARTESIAN_POINT('Ctrl Pts',(-20.5290258306396,24.6719976504383,-15.7465670946342));
#33658=CARTESIAN_POINT('Ctrl Pts',(-20.5282231626511,24.6698334279733,-15.7467107597736));
#33659=CARTESIAN_POINT('Ctrl Pts',(-20.5268379395623,24.6660861268393,-15.7469591692864));
#33660=CARTESIAN_POINT('Ctrl Pts',(-20.526254303247,24.6645034560227,-15.7470639789287));
#33661=CARTESIAN_POINT('Ctrl Pts',(-20.5250393873556,24.6612009329171,-15.7472824613604));
#33662=CARTESIAN_POINT('Ctrl Pts',(-20.5244083334255,24.6594810053201,-15.7473961202913));
#33663=CARTESIAN_POINT('Ctrl Pts',(-20.5226681805134,24.6547257104091,-15.7477100242254));
#33664=CARTESIAN_POINT('Ctrl Pts',(-20.5215621760857,24.651689200812,-15.7479100827855));
#33665=CARTESIAN_POINT('Ctrl Pts',(-20.5172485929353,24.6397907331625,-15.7486925146855));
#33666=CARTESIAN_POINT('Ctrl Pts',(-20.5140752852222,24.6309162713563,-15.7492728540497));
#33667=CARTESIAN_POINT('Ctrl Pts',(-20.4603225976594,24.4784858506931,-15.7591875811564));
#33668=CARTESIAN_POINT('Ctrl Pts',(-20.4199290283872,24.3315159038752,-15.76794053412));
#33669=CARTESIAN_POINT('Ctrl Pts',(-20.3446555373164,23.9551087271497,-15.7896078409666));
#33670=CARTESIAN_POINT('Ctrl Pts',(-20.3238532820834,23.7237700299913,-15.8022919399002));
#33671=CARTESIAN_POINT('Ctrl Pts',(-20.3295120627878,23.409686579751,-15.820422406692));
#33672=CARTESIAN_POINT('Ctrl Pts',(-20.3341672967765,23.3272680200889,-15.8252585636098));
#33673=CARTESIAN_POINT('Ctrl Pts',(-20.3459832019111,23.2030299629039,-15.8327199049889));
#33674=CARTESIAN_POINT('Ctrl Pts',(-20.3508144577647,23.1610209783441,-15.8352724468413));
#33675=CARTESIAN_POINT('Ctrl Pts',(-20.3574476667287,23.1118828273943,-15.8382967383826));
#33676=CARTESIAN_POINT('Ctrl Pts',(-20.3584493043332,23.104648380211,-15.838742976273));
#33677=CARTESIAN_POINT('Ctrl Pts',(-20.36006009167,23.0932984133447,-15.8394446316886));
#33678=CARTESIAN_POINT('Ctrl Pts',(-20.360652638206,23.0891805309549,-15.8396995224998));
#33679=CARTESIAN_POINT('Ctrl Pts',(-20.3616906898426,23.0820643951604,-15.8401405636022));
#33680=CARTESIAN_POINT('Ctrl Pts',(-20.3621324554379,23.0790655945103,-15.8403265950058));
#33681=CARTESIAN_POINT('Ctrl Pts',(-20.3630559980111,23.0728571482461,-15.8407120975768));
#33682=CARTESIAN_POINT('Ctrl Pts',(-20.3635383940179,23.0696475992777,-15.8409115882148));
#33683=CARTESIAN_POINT('Ctrl Pts',(-20.3647199623084,23.0618662066141,-15.8413957294315));
#33684=CARTESIAN_POINT('Ctrl Pts',(-20.3654241280295,23.0572951379912,-15.8416805384123));
#33685=CARTESIAN_POINT('Ctrl Pts',(-20.3680887344814,23.0402419664457,-15.8427445988345));
#33686=CARTESIAN_POINT('Ctrl Pts',(-20.3701127162663,23.0277700382262,-15.8435258679203));
#33687=CARTESIAN_POINT('Ctrl Pts',(-20.4038988980121,22.8270493759569,-15.8561497100863));
#33688=CARTESIAN_POINT('Ctrl Pts',(-20.4522468015887,22.6420120112111,-15.8685353144056));
#33689=CARTESIAN_POINT('Ctrl Pts',(-20.5813613610631,22.2819745304187,-15.8940801446763));
#33690=CARTESIAN_POINT('Ctrl Pts',(-20.6620103943619,22.1077210857707,-15.9071889968983));
#33691=CARTESIAN_POINT('Ctrl Pts',(-20.7919096143708,21.8822086118749,-15.9245945802106));
#33692=CARTESIAN_POINT('Ctrl Pts',(-20.8280523094128,21.8238536039231,-15.9291386908129));
#33693=CARTESIAN_POINT('Ctrl Pts',(-20.8871055226921,21.7349797084791,-15.9360748576416));
#33694=CARTESIAN_POINT('Ctrl Pts',(-20.9087398146202,21.7036398844754,-15.9385238354284));
#33695=CARTESIAN_POINT('Ctrl Pts',(-20.9422578632624,21.6568799505077,-15.9421737231464));
#33696=CARTESIAN_POINT('Ctrl Pts',(-20.9537334553779,21.6411730013783,-15.9433990280942));
#33697=CARTESIAN_POINT('Ctrl Pts',(-20.9677355741138,21.6223677658836,-15.9448642031369));
#33698=CARTESIAN_POINT('Ctrl Pts',(-20.9701262198227,21.6191694880023,-15.9451133266291));
#33699=CARTESIAN_POINT('Ctrl Pts',(-20.9736181469851,21.6145159430809,-15.9454757011331));
#33700=CARTESIAN_POINT('Ctrl Pts',(-20.974714718062,21.6130571715016,-15.9455892816566));
#33701=CARTESIAN_POINT('Ctrl Pts',(-20.9768360361437,21.6102401611601,-15.9458085849882));
#33702=CARTESIAN_POINT('Ctrl Pts',(-20.9778606208028,21.6088818009391,-15.9459143192462));
#33703=CARTESIAN_POINT('Ctrl Pts',(-20.9799648509826,21.6060966731937,-15.9461310837908));
#33704=CARTESIAN_POINT('Ctrl Pts',(-20.9810446066318,21.604669996412,-15.9462421057181));
#33705=CARTESIAN_POINT('Ctrl Pts',(-20.9836433314752,21.6012422476326,-15.9465088132865));
#33706=CARTESIAN_POINT('Ctrl Pts',(-20.9851634564067,21.5992420473637,-15.9466644169903));
#33707=CARTESIAN_POINT('Ctrl Pts',(-20.990701834886,21.5919722381826,-15.9472298690332));
#33708=CARTESIAN_POINT('Ctrl Pts',(-20.9947340366302,21.5867132016198,-15.9476387377724));
#33709=CARTESIAN_POINT('Ctrl Pts',(-21.0628267932135,21.4984676360012,-15.9544970809675));
#33710=CARTESIAN_POINT('Ctrl Pts',(-21.1308908243764,21.4186329001386,-15.9606666054038));
#33711=CARTESIAN_POINT('Ctrl Pts',(-21.3653305526648,21.1693797206497,-15.9803431369683));
#33712=CARTESIAN_POINT('Ctrl Pts',(-21.5465295370092,21.0149919761516,-15.9932609415746));
#33713=CARTESIAN_POINT('Ctrl Pts',(-21.8409155786779,20.8156124909234,-16.0134698080465));
#33714=CARTESIAN_POINT('Ctrl Pts',(-21.9423463705577,20.754769997483,-16.0203038930105));
#33715=CARTESIAN_POINT('Ctrl Pts',(-22.0923006039046,20.6756864330998,-16.0303942376606));
#33716=CARTESIAN_POINT('Ctrl Pts',(-22.1382823152275,20.6528237184469,-16.0334859214619));
#33717=CARTESIAN_POINT('Ctrl Pts',(-22.1919981881076,20.6276978186748,-16.0371017974909));
#33718=CARTESIAN_POINT('Ctrl Pts',(-22.1992201488088,20.6243522580917,-16.0375880242147));
#33719=CARTESIAN_POINT('Ctrl Pts',(-22.2102385444714,20.6192974978878,-16.0383300009811));
#33720=CARTESIAN_POINT('Ctrl Pts',(-22.2140260571149,20.6175688282371,-16.0385850784093));
#33721=CARTESIAN_POINT('Ctrl Pts',(-22.220577225028,20.6145941163198,-16.0390263303496));
#33722=CARTESIAN_POINT('Ctrl Pts',(-22.2233393148803,20.6133446223686,-16.039212385636));
#33723=CARTESIAN_POINT('Ctrl Pts',(-22.2290609536418,20.6107660285708,-16.0395978311382));
#33724=CARTESIAN_POINT('Ctrl Pts',(-22.2320207537833,20.6094374971269,-16.0397972406654));
#33725=CARTESIAN_POINT('Ctrl Pts',(-22.2392004843591,20.6062278310157,-16.0402810061358));
#33726=CARTESIAN_POINT('Ctrl Pts',(-22.2434224551925,20.6043513011993,-16.0405655199615));
#33727=CARTESIAN_POINT('Ctrl Pts',(-22.2591772031941,20.5973893575433,-16.0416273753202));
#33728=CARTESIAN_POINT('Ctrl Pts',(-22.2707356304771,20.5923625876015,-16.0424067237675));
#33729=CARTESIAN_POINT('Ctrl Pts',(-22.4681267831465,20.5078904893647,-16.0557225632843));
#33730=CARTESIAN_POINT('Ctrl Pts',(-22.6609609018353,20.4460464391205,-16.0688711497315));
#33731=CARTESIAN_POINT('Ctrl Pts',(-23.1468802572785,20.3392211500691,-16.1021862759221));
#33732=CARTESIAN_POINT('Ctrl Pts',(-23.442832925527,20.3157658377569,-16.1226991669451));
#33733=CARTESIAN_POINT('Ctrl Pts',(-23.7461048117153,20.3334485322113,-16.141857659537));
#33734=CARTESIAN_POINT('Ctrl Pts',(-23.754366928766,20.333962214715,-16.1423780630931));
#33735=CARTESIAN_POINT('Ctrl Pts',(-23.7686545929358,20.3349058020991,-16.1432752312063));
#33736=CARTESIAN_POINT('Ctrl Pts',(-23.7746810332003,20.335320821534,-16.143652799318));
#33737=CARTESIAN_POINT('Ctrl Pts',(-23.7833016107457,20.3359388476615,-16.1441916423399));
#33738=CARTESIAN_POINT('Ctrl Pts',(-23.785896677357,20.3361280522541,-16.1443536886514));
#33739=CARTESIAN_POINT('Ctrl Pts',(-23.7903999578517,20.3364618667089,-16.1446346060725));
#33740=CARTESIAN_POINT('Ctrl Pts',(-23.7923082747745,20.336605033609,-16.1447535590887));
#33741=CARTESIAN_POINT('Ctrl Pts',(-23.7959660444374,20.3368827255875,-16.1449813905479));
#33742=CARTESIAN_POINT('Ctrl Pts',(-23.7977155120714,20.3370169794008,-16.1450902843391));
#33743=CARTESIAN_POINT('Ctrl Pts',(-23.8018383681433,20.3373367536569,-16.1453467316237));
#33744=CARTESIAN_POINT('Ctrl Pts',(-23.8042116663202,20.3375234755974,-16.1454942168495));
#33745=CARTESIAN_POINT('Ctrl Pts',(-23.8112262394054,20.3380831764403,-16.1459297277339));
#33746=CARTESIAN_POINT('Ctrl Pts',(-23.8158669407877,20.3384635863751,-16.1462173356499));
#33747=CARTESIAN_POINT('Ctrl Pts',(-23.8564646428799,20.3418800741789,-16.1487289815435));
#33748=CARTESIAN_POINT('Ctrl Pts',(-23.8923709435871,20.3455099612613,-16.1509201766677));
#33749=CARTESIAN_POINT('Ctrl Pts',(-23.9335312281696,20.3503707044785,-16.153405012533));
#33750=CARTESIAN_POINT('Ctrl Pts',(-23.938850403698,20.351012315336,-16.153725610894));
#33751=CARTESIAN_POINT('Ctrl Pts',(-24.2412437156542,20.3882529662706,-16.1719232534179));
#33752=CARTESIAN_POINT('Ctrl Pts',(-24.5318136528108,20.4660505545078,-16.1879719027631));
#33753=CARTESIAN_POINT('Ctrl Pts',(-24.960353549938,20.6476173661421,-16.2143954608027));
#33754=CARTESIAN_POINT('Ctrl Pts',(-25.1079528844729,20.7240831302503,-16.2240469985579));
#33755=CARTESIAN_POINT('Ctrl Pts',(-25.2600807065299,20.8184444551972,-16.2349232932918));
#33756=CARTESIAN_POINT('Ctrl Pts',(-25.271124970129,20.8253881686354,-16.2357183467143));
#33757=CARTESIAN_POINT('Ctrl Pts',(-25.2864246415602,20.8351374436919,-16.2368274579456));
#33758=CARTESIAN_POINT('Ctrl Pts',(-25.2907161168922,20.837886397799,-16.2371394080807));
#33759=CARTESIAN_POINT('Ctrl Pts',(-25.2979466570163,20.8425422294161,-16.2376664454253));
#33760=CARTESIAN_POINT('Ctrl Pts',(-25.3008891757644,20.8444437474241,-16.2378813321513));
#33761=CARTESIAN_POINT('Ctrl Pts',(-25.3067032611842,20.8482143867174,-16.2383067291597));
#33762=CARTESIAN_POINT('Ctrl Pts',(-25.309574959735,20.8500832969837,-16.2385172313467));
#33763=CARTESIAN_POINT('Ctrl Pts',(-25.3158946897643,20.8542105584941,-16.2389813443974));
#33764=CARTESIAN_POINT('Ctrl Pts',(-25.3193413764872,20.8564709498664,-16.2392350316947));
#33765=CARTESIAN_POINT('Ctrl Pts',(-25.3313480136562,20.8643780735084,-16.2401207462866));
#33766=CARTESIAN_POINT('Ctrl Pts',(-25.3398852728665,20.8700589997226,-16.2407540605579));
#33767=CARTESIAN_POINT('Ctrl Pts',(-25.4263129262855,20.9281673853676,-16.2472017497701));
#33768=CARTESIAN_POINT('Ctrl Pts',(-25.5018967105281,20.9839292577078,-16.253142943193));
#33769=CARTESIAN_POINT('Ctrl Pts',(-25.8171293609277,21.2384794146637,-16.2793060483272));
#33770=CARTESIAN_POINT('Ctrl Pts',(-26.0296937018015,21.4681058460494,-16.3008083782085));
#33771=CARTESIAN_POINT('Ctrl Pts',(-26.259861311251,21.8029171853361,-16.3278215541238));
#33772=CARTESIAN_POINT('Ctrl Pts',(-26.3102439052869,21.8836355934166,-16.3340369780062));
#33773=CARTESIAN_POINT('Ctrl Pts',(-26.361313971744,21.9741406483432,-16.3405955626054));
#33774=CARTESIAN_POINT('Ctrl Pts',(-26.3656096393641,21.9818267447743,-16.3411494013173));
#33775=CARTESIAN_POINT('Ctrl Pts',(-26.3729687008238,21.9951217231519,-16.3421018557458));
#33776=CARTESIAN_POINT('Ctrl Pts',(-26.3760469847028,22.00072224346,-16.3425013893594));
#33777=CARTESIAN_POINT('Ctrl Pts',(-26.3803874956574,22.0086751659799,-16.3430663096522));
#33778=CARTESIAN_POINT('Ctrl Pts',(-26.381663464712,22.0110199900551,-16.3432325709968));
#33779=CARTESIAN_POINT('Ctrl Pts',(-26.3838503724448,22.0150507496727,-16.3435178584734));
#33780=CARTESIAN_POINT('Ctrl Pts',(-26.3847627220969,22.0167359145028,-16.3436369756159));
#33781=CARTESIAN_POINT('Ctrl Pts',(-26.386506143618,22.0199629906327,-16.3438647864181));
#33782=CARTESIAN_POINT('Ctrl Pts',(-26.3873374602829,22.0215047635375,-16.3439734959809));
#33783=CARTESIAN_POINT('Ctrl Pts',(-26.3892900573071,22.0251331586952,-16.3442290290336));
#33784=CARTESIAN_POINT('Ctrl Pts',(-26.3904102967319,22.0272203444061,-16.3443757854542));
#33785=CARTESIAN_POINT('Ctrl Pts',(-26.3937040272258,22.0333733637871,-16.3448077351599));
#33786=CARTESIAN_POINT('Ctrl Pts',(-26.3958711079054,22.0374426504409,-16.3450925202806));
#33787=CARTESIAN_POINT('Ctrl Pts',(-26.414361651163,22.0723440149388,-16.347527615613));
#33788=CARTESIAN_POINT('Ctrl Pts',(-26.4301930135577,22.1034361316098,-16.3496472474607));
#33789=CARTESIAN_POINT('Ctrl Pts',(-26.4478211484017,22.1394934480009,-16.3520557123517));
#33790=CARTESIAN_POINT('Ctrl Pts',(-26.45011366721,22.1442118223947,-16.3523699102967));
#33791=CARTESIAN_POINT('Ctrl Pts',(-26.455551299867,22.1554732185961,-16.3531175543574));
#33792=CARTESIAN_POINT('Ctrl Pts',(-26.4586858589235,22.1620213378661,-16.3535504740378));
#33793=CARTESIAN_POINT('Ctrl Pts',(-26.5894491268685,22.4375737887252,-16.3716946149772));
#33794=CARTESIAN_POINT('Ctrl Pts',(-26.6792235739005,22.7229917398335,-16.3876603733281));
#33795=CARTESIAN_POINT('Ctrl Pts',(-26.7393058296764,23.0808990059564,-16.4082902284006));
#33796=CARTESIAN_POINT('Ctrl Pts',(-26.7481336586921,23.1453953544504,-16.4120249039404));
#33797=CARTESIAN_POINT('Ctrl Pts',(-26.7641721297485,23.2965074438916,-16.4208646940189));
#33798=CARTESIAN_POINT('Ctrl Pts',(-26.7698437548746,23.3832313337948,-16.4260067265475));
#33799=CARTESIAN_POINT('Ctrl Pts',(-26.7725208419207,23.4908014556169,-16.4325142843219));
#33800=CARTESIAN_POINT('Ctrl Pts',(-26.7728366394631,23.5115339232404,-16.4337743854439));
#33801=CARTESIAN_POINT('Ctrl Pts',(-26.7729860115577,23.5382997794761,-16.4354092076705));
#33802=CARTESIAN_POINT('Ctrl Pts',(-26.7730027387142,23.5443319836837,-16.4357781717786));
#33803=CARTESIAN_POINT('Ctrl Pts',(-26.773002414159,23.5537014185231,-16.4363520874291));
#33804=CARTESIAN_POINT('Ctrl Pts',(-26.7729971148261,23.5570386577689,-16.4365566698283));
#33805=CARTESIAN_POINT('Ctrl Pts',(-26.7729761171642,23.5637231980577,-16.4369667804481));
#33806=CARTESIAN_POINT('Ctrl Pts',(-26.7729603873923,23.5670704948622,-16.4371723094054));
#33807=CARTESIAN_POINT('Ctrl Pts',(-26.7729135993226,23.5745478893007,-16.4376318042383));
#33808=CARTESIAN_POINT('Ctrl Pts',(-26.7728798163901,23.5786779584991,-16.4378858553278));
#33809=CARTESIAN_POINT('Ctrl Pts',(-26.772757656836,23.5907702554031,-16.4386304315405));
#33810=CARTESIAN_POINT('Ctrl Pts',(-26.7726477104821,23.598732191346,-16.4391216330619));
#33811=CARTESIAN_POINT('Ctrl Pts',(-26.7716183296428,23.6575002038599,-16.4427543688305));
#33812=CARTESIAN_POINT('Ctrl Pts',(-26.7695269415026,23.7082761538649,-16.4459325224983));
#33813=CARTESIAN_POINT('Ctrl Pts',(-26.7587256799193,23.8746980126637,-16.4564868790752));
#33814=CARTESIAN_POINT('Ctrl Pts',(-26.7449758354435,23.9899144930387,-16.464016600083));
#33815=CARTESIAN_POINT('Ctrl Pts',(-26.6808123863661,24.3576965711887,-16.4887339943904));
#33816=CARTESIAN_POINT('Ctrl Pts',(-26.6063627843755,24.6050253632018,-16.5064887308816));
#33817=CARTESIAN_POINT('Ctrl Pts',(-26.4680266309504,24.921554203162,-16.5293187768705));
#33818=CARTESIAN_POINT('Ctrl Pts',(-26.4294602260831,25.0007835899275,-16.535032637019));
#33819=CARTESIAN_POINT('Ctrl Pts',(-26.3846658489233,25.0839602755355,-16.5409548553504));
#33820=CARTESIAN_POINT('Ctrl Pts',(-26.3816229165237,25.0895705761438,-16.5413539259994));
#33821=CARTESIAN_POINT('Ctrl Pts',(-26.3773779963793,25.0973418255469,-16.5419061338582));
#33822=CARTESIAN_POINT('Ctrl Pts',(-26.3761901840895,25.099510438274,-16.5420601684062));
#33823=CARTESIAN_POINT('Ctrl Pts',(-26.3741436695224,25.103236616458,-16.5423247253604));
#33824=CARTESIAN_POINT('Ctrl Pts',(-26.3732861738627,25.1047948376656,-16.5424353252259));
#33825=CARTESIAN_POINT('Ctrl Pts',(-26.3715116258743,25.1080131946393,-16.5426636889085));
#33826=CARTESIAN_POINT('Ctrl Pts',(-26.3705943997094,25.1096732276734,-16.5427814405981));
#33827=CARTESIAN_POINT('Ctrl Pts',(-26.3684365167118,25.1135705203405,-16.5430577998073));
#33828=CARTESIAN_POINT('Ctrl Pts',(-26.3671946571006,25.1158071200922,-16.5432163296278));
#33829=CARTESIAN_POINT('Ctrl Pts',(-26.3631487881025,25.1230733647321,-16.5437311441233));
#33830=CARTESIAN_POINT('Ctrl Pts',(-26.3603339406385,25.128097010239,-16.5440867337083));
#33831=CARTESIAN_POINT('Ctrl Pts',(-26.2763178414771,25.2771022062031,-16.5546246028893));
#33832=CARTESIAN_POINT('Ctrl Pts',(-26.1841583954558,25.4146556912969,-16.5641021811261));
#33833=CARTESIAN_POINT('Ctrl Pts',(-25.8767988034859,25.8048219349782,-16.592081973591));
#33834=CARTESIAN_POINT('Ctrl Pts',(-25.6328827139552,26.0318930769095,-16.6101488225876));
#33835=CARTESIAN_POINT('Ctrl Pts',(-25.3419746128606,26.2291058475531,-16.6314061013047));
#33836=CARTESIAN_POINT('Ctrl Pts',(-25.3252005728499,26.2402492838476,-16.632629899594));
#33837=CARTESIAN_POINT('Ctrl Pts',(-25.3031077381031,26.2546295241833,-16.6342396624682));
#33838=CARTESIAN_POINT('Ctrl Pts',(-25.297882193997,26.2580093255589,-16.6346202628348));
#33839=CARTESIAN_POINT('Ctrl Pts',(-25.2898070768455,26.2631990742448,-16.6352081902425));
#33840=CARTESIAN_POINT('Ctrl Pts',(-25.2869643745615,26.2650197285271,-16.6354151177125));
#33841=CARTESIAN_POINT('Ctrl Pts',(-25.2813005818393,26.2686346587308,-16.6358273184942));
#33842=CARTESIAN_POINT('Ctrl Pts',(-25.2784795492928,26.2704290178825,-16.6360325883688));
#33843=CARTESIAN_POINT('Ctrl Pts',(-25.2722238197497,26.2743944068842,-16.636487695241));
#33844=CARTESIAN_POINT('Ctrl Pts',(-25.268787802895,26.2765633346748,-16.6367376098422));
#33845=CARTESIAN_POINT('Ctrl Pts',(-25.2590035420358,26.2827136382462,-16.6374491002396));
#33846=CARTESIAN_POINT('Ctrl Pts',(-25.2526455321466,26.2866793596312,-16.6379112545568));
#33847=CARTESIAN_POINT('Ctrl Pts',(-25.2114799432765,26.3121568338247,-16.6409023958203));
#33848=CARTESIAN_POINT('Ctrl Pts',(-25.1762805051653,26.3330253696343,-16.6434549231763));
#33849=CARTESIAN_POINT('Ctrl Pts',(-25.0703427078755,26.3931359796786,-16.6511263575044));
#33850=CARTESIAN_POINT('Ctrl Pts',(-24.9985184259472,26.4303887257047,-16.6563143504873));
#33851=CARTESIAN_POINT('Ctrl Pts',(-24.6870847592688,26.5773222196769,-16.6787580811849));
#33852=CARTESIAN_POINT('Ctrl Pts',(-24.4359223040316,26.6600908345066,-16.6968390638425));
#33853=CARTESIAN_POINT('Ctrl Pts',(-24.0892232617592,26.7288899825186,-16.720513163993));
#33854=CARTESIAN_POINT('Ctrl Pts',(-24.0001980434589,26.742708826642,-16.7264712575149));
#33855=CARTESIAN_POINT('Ctrl Pts',(-23.8715756730833,26.7571855592581,-16.7348055624111));
#33856=CARTESIAN_POINT('Ctrl Pts',(-23.8323673976582,26.7608723406366,-16.7373097274845));
#33857=CARTESIAN_POINT('Ctrl Pts',(-23.7883383201914,26.7641995623351,-16.7400737216579));
#33858=CARTESIAN_POINT('Ctrl Pts',(-23.7835765542512,26.7645487625424,-16.7403720194128));
#33859=CARTESIAN_POINT('Ctrl Pts',(-23.7764092124176,26.765058362607,-16.740820047701));
#33860=CARTESIAN_POINT('Ctrl Pts',(-23.7740042304935,26.7652266454445,-16.7409702188702));
#33861=CARTESIAN_POINT('Ctrl Pts',(-23.7698408474697,26.7655132738445,-16.7412299019444));
#33862=CARTESIAN_POINT('Ctrl Pts',(-23.7680825384887,26.765632875699,-16.7413394849364));
#33863=CARTESIAN_POINT('Ctrl Pts',(-23.7644209602992,26.7658789224754,-16.7415675004118));
#33864=CARTESIAN_POINT('Ctrl Pts',(-23.7625176790386,26.766005119836,-16.7416859182553));
#33865=CARTESIAN_POINT('Ctrl Pts',(-23.7580512997036,26.7662972813061,-16.741963564001));
#33866=CARTESIAN_POINT('Ctrl Pts',(-23.7554881059359,26.7664618716888,-16.7421227139573));
#33867=CARTESIAN_POINT('Ctrl Pts',(-23.7470844208006,26.7669914104831,-16.7426438974629));
#33868=CARTESIAN_POINT('Ctrl Pts',(-23.7412430883274,26.7673435181961,-16.7430052093063));
#33869=CARTESIAN_POINT('Ctrl Pts',(-23.727455781793,26.7681369147324,-16.743855820633));
#33870=CARTESIAN_POINT('Ctrl Pts',(-23.719509025633,26.7685646882122,-16.7443443790117));
#33871=CARTESIAN_POINT('Ctrl Pts',(-23.4406632197143,26.7825392590476,-16.7614297924199));
#33872=CARTESIAN_POINT('Ctrl Pts',(-23.1690829620679,26.761864679703,-16.7762181705965));
#33873=CARTESIAN_POINT('Ctrl Pts',(-22.7559390570677,26.6772000553047,-16.799854726454));
#33874=CARTESIAN_POINT('Ctrl Pts',(-22.6109154525277,26.6367350842044,-16.8083699612486));
#33875=CARTESIAN_POINT('Ctrl Pts',(-22.4558341201495,26.5815177652751,-16.8180288959535));
#33876=CARTESIAN_POINT('Ctrl Pts',(-22.4424432886137,26.5766496054537,-16.8188674544971));
#33877=CARTESIAN_POINT('Ctrl Pts',(-22.4223921379274,26.5692092160247,-16.8201301803131));
#33878=CARTESIAN_POINT('Ctrl Pts',(-22.4157072628945,26.5667033537038,-16.8205523497294));
#33879=CARTESIAN_POINT('Ctrl Pts',(-22.4052623349331,26.5627483822028,-16.82121387029));
#33880=CARTESIAN_POINT('Ctrl Pts',(-22.4014965551695,26.5613143886148,-16.8214527586597));
#33881=CARTESIAN_POINT('Ctrl Pts',(-22.3938797749693,26.5583975812164,-16.8219367304857));
#33882=CARTESIAN_POINT('Ctrl Pts',(-22.3900289140356,26.5569144262648,-16.8221818240965));
#33883=CARTESIAN_POINT('Ctrl Pts',(-22.3369601884303,26.5363579290019,-16.8255651577632));
#33884=CARTESIAN_POINT('Ctrl Pts',(-22.2882176655084,26.5160865212968,-16.8287405286875));
#33885=CARTESIAN_POINT('Ctrl Pts',(-22.2320260170298,26.4910810776542,-16.8324886683763));
#33886=CARTESIAN_POINT('Ctrl Pts',(-22.2240695523943,26.4875016501306,-16.8330214551079));
#33887=CARTESIAN_POINT('Ctrl Pts',(-22.2122258440204,26.4821155093004,-16.8338176672126));
#33888=CARTESIAN_POINT('Ctrl Pts',(-22.2083274655846,26.4803332563587,-16.8340802486095));
#33889=CARTESIAN_POINT('Ctrl Pts',(-22.2013775261303,26.4771391176962,-16.8345492823342));
#33890=CARTESIAN_POINT('Ctrl Pts',(-22.1983245914669,26.4757302212776,-16.8347556310788));
#33891=CARTESIAN_POINT('Ctrl Pts',(-22.1918895131608,26.4727482777622,-16.8351912451679));
#33892=CARTESIAN_POINT('Ctrl Pts',(-22.1885078865786,26.4711741323568,-16.8354205483232));
#33893=CARTESIAN_POINT('Ctrl Pts',(-22.1795755904479,26.4669972701619,-16.8360272661396));
#33894=CARTESIAN_POINT('Ctrl Pts',(-22.1740296213429,26.4643845889002,-16.8364050261754));
#33895=CARTESIAN_POINT('Ctrl Pts',(-22.1493006580692,26.4526485477194,-16.8380941713147));
#33896=CARTESIAN_POINT('Ctrl Pts',(-22.1302010410033,26.443351651158,-16.8394115859042));
#33897=CARTESIAN_POINT('Ctrl Pts',(-22.0991025237082,26.4278320466885,-16.8415780498589));
#33898=CARTESIAN_POINT('Ctrl Pts',(-22.0870492666874,26.4217219015699,-16.8424230571167));
#33899=CARTESIAN_POINT('Ctrl Pts',(-22.0750360036057,26.4155367685116,-16.8432706449041));
#33900=CARTESIAN_POINT('',(-26.7730012036304,23.553178285231,-16.6852117869365));
#33901=CARTESIAN_POINT('Ctrl Pts',(-22.0750360832114,26.4155368094973,-17.0912958973716));
#33902=CARTESIAN_POINT('Ctrl Pts',(-22.1535668768981,26.4559690693804,-17.0863106787744));
#33903=CARTESIAN_POINT('Ctrl Pts',(-22.233752977376,26.4931692513465,-17.0813837806402));
#33904=CARTESIAN_POINT('Ctrl Pts',(-22.4752708579841,26.5933580093501,-17.0667708531272));
#33905=CARTESIAN_POINT('Ctrl Pts',(-22.6402209590496,26.6466879184113,-17.0570632839845));
#33906=CARTESIAN_POINT('Ctrl Pts',(-22.8359745711018,26.692976406064,-17.0453123444403));
#33907=CARTESIAN_POINT('Ctrl Pts',(-22.863389019571,26.6990816482408,-17.0436620881841));
#33908=CARTESIAN_POINT('Ctrl Pts',(-22.9017596647664,26.7071019295469,-17.0413440422702));
#33909=CARTESIAN_POINT('Ctrl Pts',(-22.9126517240969,26.7093198505397,-17.0406851087459));
#33910=CARTESIAN_POINT('Ctrl Pts',(-22.9759360276291,26.7218656428443,-17.0368508300875));
#33911=CARTESIAN_POINT('Ctrl Pts',(-23.0285645596691,26.7309459025835,-17.0336389714329));
#33912=CARTESIAN_POINT('Ctrl Pts',(-23.0900548790222,26.7399879986226,-17.0298514728927));
#33913=CARTESIAN_POINT('Ctrl Pts',(-23.0987227205324,26.7412265296696,-17.0293167811369));
#33914=CARTESIAN_POINT('Ctrl Pts',(-23.1116476123205,26.7430196256445,-17.0285182651049));
#33915=CARTESIAN_POINT('Ctrl Pts',(-23.1159009478169,26.7436010395792,-17.0282552920034));
#33916=CARTESIAN_POINT('Ctrl Pts',(-23.1234886089753,26.7446228027192,-17.0277858105125));
#33917=CARTESIAN_POINT('Ctrl Pts',(-23.1268224923757,26.7450664348518,-17.0275794064221));
#33918=CARTESIAN_POINT('Ctrl Pts',(-23.1338521141308,26.7459906536671,-17.0271439351751));
#33919=CARTESIAN_POINT('Ctrl Pts',(-23.1375480016303,26.746470049739,-17.0269148306475));
#33920=CARTESIAN_POINT('Ctrl Pts',(-23.1473109141334,26.7477191877687,-17.0263092326643));
#33921=CARTESIAN_POINT('Ctrl Pts',(-23.1533792914866,26.7484780700596,-17.0259323961525));
#33922=CARTESIAN_POINT('Ctrl Pts',(-23.1803935549792,26.751778275601,-17.0242529900768));
#33923=CARTESIAN_POINT('Ctrl Pts',(-23.2013615593792,26.7541310885205,-17.0229444762228));
#33924=CARTESIAN_POINT('Ctrl Pts',(-23.340202739262,26.7683313099536,-17.0142455579066));
#33925=CARTESIAN_POINT('Ctrl Pts',(-23.4586156390194,26.7738760817245,-17.0066572019617));
#33926=CARTESIAN_POINT('Ctrl Pts',(-23.6030754443777,26.7726746764825,-16.9971890913247));
#33927=CARTESIAN_POINT('Ctrl Pts',(-23.6290930820044,26.772143103359,-16.9954757663598));
#33928=CARTESIAN_POINT('Ctrl Pts',(-23.8122754572498,26.7661803218788,-16.9833583251791));
#33929=CARTESIAN_POINT('Ctrl Pts',(-23.9688553027553,26.7495669811217,-16.9727033783324));
#33930=CARTESIAN_POINT('Ctrl Pts',(-24.3067094341909,26.6884878975699,-16.9494739427274));
#33931=CARTESIAN_POINT('Ctrl Pts',(-24.486647441895,26.6395778219922,-16.9369462902151));
#33932=CARTESIAN_POINT('Ctrl Pts',(-24.6719702688918,26.5715095994221,-16.9245070861992));
#33933=CARTESIAN_POINT('Ctrl Pts',(-24.6825445666759,26.5675625435694,-16.9237990433152));
#33934=CARTESIAN_POINT('Ctrl Pts',(-24.6963458025573,26.5623282016901,-16.9228773910607));
#33935=CARTESIAN_POINT('Ctrl Pts',(-24.6995915345834,26.5610911995753,-16.9226608184342));
#33936=CARTESIAN_POINT('Ctrl Pts',(-24.7045917194712,26.5591762827424,-16.9223274620397));
#33937=CARTESIAN_POINT('Ctrl Pts',(-24.7063475764904,26.5585020804352,-16.9222104549456));
#33938=CARTESIAN_POINT('Ctrl Pts',(-24.7096697492131,26.5572231163988,-16.921989174708));
#33939=CARTESIAN_POINT('Ctrl Pts',(-24.7112361746242,26.556618670812,-16.9218848833334));
#33940=CARTESIAN_POINT('Ctrl Pts',(-24.7148741016107,26.5552116157129,-16.9216427740848));
#33941=CARTESIAN_POINT('Ctrl Pts',(-24.7169452427108,26.5544080895629,-16.921505012633));
#33942=CARTESIAN_POINT('Ctrl Pts',(-24.7212064772963,26.5527498167611,-16.9212217307855));
#33943=CARTESIAN_POINT('Ctrl Pts',(-24.7233964704818,26.5518948136001,-16.9210762259824));
#33944=CARTESIAN_POINT('Ctrl Pts',(-24.7344492553768,26.547565711922,-16.9203422822242));
#33945=CARTESIAN_POINT('Ctrl Pts',(-24.7432976825977,26.5440547051928,-16.9197560527474));
#33946=CARTESIAN_POINT('Ctrl Pts',(-24.7657919765879,26.5350135280801,-16.9182688468553));
#33947=CARTESIAN_POINT('Ctrl Pts',(-24.7794159032692,26.5294288897283,-16.9173710157967));
#33948=CARTESIAN_POINT('Ctrl Pts',(-24.8353207454088,26.506063927783,-16.9136969541139));
#33949=CARTESIAN_POINT('Ctrl Pts',(-24.8772601048056,26.4874744665159,-16.9109646321013));
#33950=CARTESIAN_POINT('Ctrl Pts',(-24.9970029090544,26.4313102961489,-16.9031933193554));
#33951=CARTESIAN_POINT('Ctrl Pts',(-25.0737138454802,26.3914931168652,-16.8982513873834));
#33952=CARTESIAN_POINT('Ctrl Pts',(-25.2138467423114,26.3114469215322,-16.8891286217551));
#33953=CARTESIAN_POINT('Ctrl Pts',(-25.277640420067,26.2719930911369,-16.8849363828752));
#33954=CARTESIAN_POINT('Ctrl Pts',(-25.5665349624495,26.0790715053874,-16.8655242993437));
#33955=CARTESIAN_POINT('Ctrl Pts',(-25.772939675415,25.8997111854494,-16.8502916386441));
#33956=CARTESIAN_POINT('Ctrl Pts',(-25.9660425585434,25.6834158686752,-16.8327277529319));
#33957=CARTESIAN_POINT('Ctrl Pts',(-25.9776550352329,25.6701922343086,-16.8316572857906));
#33958=CARTESIAN_POINT('Ctrl Pts',(-25.993013206432,25.6524115704127,-16.8302220678694));
#33959=CARTESIAN_POINT('Ctrl Pts',(-25.9968556895914,25.6479382386457,-16.8298613363571));
#33960=CARTESIAN_POINT('Ctrl Pts',(-26.0028358299159,25.640937511541,-16.8292973232686));
#33961=CARTESIAN_POINT('Ctrl Pts',(-26.0049819212287,25.6384173105604,-16.8290943899135));
#33962=CARTESIAN_POINT('Ctrl Pts',(-26.0090763740541,25.6335940723103,-16.8287062107611));
#33963=CARTESIAN_POINT('Ctrl Pts',(-26.0110253933173,25.6312915957232,-16.8285209922938));
#33964=CARTESIAN_POINT('Ctrl Pts',(-26.0155698452952,25.6259076902571,-16.8280880953873));
#33965=CARTESIAN_POINT('Ctrl Pts',(-26.018162734055,25.6228241292174,-16.8278403130069));
#33966=CARTESIAN_POINT('Ctrl Pts',(-26.0255559181731,25.6139983308701,-16.8271315405065));
#33967=CARTESIAN_POINT('Ctrl Pts',(-26.0303419778832,25.6082442508509,-16.8266699697743));
#33968=CARTESIAN_POINT('Ctrl Pts',(-26.0409898359572,25.5953516887241,-16.8256369118406));
#33969=CARTESIAN_POINT('Ctrl Pts',(-26.0468410583227,25.5882045936378,-16.8250649994524));
#33970=CARTESIAN_POINT('Ctrl Pts',(-26.0907402773733,25.5341102073467,-16.8207419968735));
#33971=CARTESIAN_POINT('Ctrl Pts',(-26.1274895919554,25.4861289739368,-16.8169391030921));
#33972=CARTESIAN_POINT('Ctrl Pts',(-26.2438107248451,25.3250693831589,-16.8042645727324));
#33973=CARTESIAN_POINT('Ctrl Pts',(-26.3174495983621,25.207914382771,-16.7951787702345));
#33974=CARTESIAN_POINT('Ctrl Pts',(-26.4071199249425,25.0425381886739,-16.7825878435136));
#33975=CARTESIAN_POINT('Ctrl Pts',(-26.4298836294418,24.9981241856403,-16.7792291414005));
#33976=CARTESIAN_POINT('Ctrl Pts',(-26.4623134575627,24.9310579691324,-16.7741995481262));
#33977=CARTESIAN_POINT('Ctrl Pts',(-26.4727665624012,24.9087937421993,-16.7725366615279));
#33978=CARTESIAN_POINT('Ctrl Pts',(-26.494781266265,24.8604740896805,-16.7689441812351));
#33979=CARTESIAN_POINT('Ctrl Pts',(-26.5062541530103,24.8343804113196,-16.767014340597));
#33980=CARTESIAN_POINT('Ctrl Pts',(-26.5817546356709,24.6562882782503,-16.7539218144734));
#33981=CARTESIAN_POINT('Ctrl Pts',(-26.6343841769804,24.4997061500629,-16.7427837206607));
#33982=CARTESIAN_POINT('Ctrl Pts',(-26.6842960497413,24.3021781936186,-16.7296703432913));
#33983=CARTESIAN_POINT('Ctrl Pts',(-26.6931163120391,24.2644153756936,-16.7272051004348));
#33984=CARTESIAN_POINT('Ctrl Pts',(-26.702250877742,24.2218525523555,-16.7244801587211));
#33985=CARTESIAN_POINT('Ctrl Pts',(-26.703238119652,24.2172023379461,-16.7241831601281));
#33986=CARTESIAN_POINT('Ctrl Pts',(-26.7047094542041,24.2101956153712,-16.7237367519101));
#33987=CARTESIAN_POINT('Ctrl Pts',(-26.7052011981482,24.207840747675,-16.7235869060832));
#33988=CARTESIAN_POINT('Ctrl Pts',(-26.706048362062,24.2037610174578,-16.7233276281163));
#33989=CARTESIAN_POINT('Ctrl Pts',(-26.7064050048825,24.2020364145528,-16.7232181254253));
#33990=CARTESIAN_POINT('Ctrl Pts',(-26.7071452216315,24.1984421255273,-16.7229901187458));
#33991=CARTESIAN_POINT('Ctrl Pts',(-26.7075285478719,24.1965723929244,-16.7228716296236));
#33992=CARTESIAN_POINT('Ctrl Pts',(-26.7082882494431,24.1928500276516,-16.7226359698331));
#33993=CARTESIAN_POINT('Ctrl Pts',(-26.7086646565208,24.1909973999378,-16.722518797222));
#33994=CARTESIAN_POINT('Ctrl Pts',(-26.7095425181369,24.1866571073863,-16.722244556627));
#33995=CARTESIAN_POINT('Ctrl Pts',(-26.7100426658605,24.1841691748965,-16.7220875636834));
#33996=CARTESIAN_POINT('Ctrl Pts',(-26.711345021966,24.1776509039523,-16.7216767841636));
#33997=CARTESIAN_POINT('Ctrl Pts',(-26.7121424643921,24.1736196013311,-16.7214232680318));
#33998=CARTESIAN_POINT('Ctrl Pts',(-26.7526918072996,23.9665511448661,-16.7084283403808));
#33999=CARTESIAN_POINT('Ctrl Pts',(-26.772813325684,23.7601278435454,-16.6967895284045));
#34000=CARTESIAN_POINT('Ctrl Pts',(-26.7730012036304,23.553178285231,-16.6852117869365));
#34001=CARTESIAN_POINT('Ctrl Pts',(-26.7730012021961,23.5531798646698,-16.6852118752978));
#34002=CARTESIAN_POINT('Ctrl Pts',(-26.7731886828151,23.3467793900092,-16.6736648516152));
#34003=CARTESIAN_POINT('Ctrl Pts',(-26.7535484417044,23.1408458469785,-16.6622156702365));
#34004=CARTESIAN_POINT('Ctrl Pts',(-26.7017859055637,22.8732506738851,-16.6463314591706));
#34005=CARTESIAN_POINT('Ctrl Pts',(-26.6872256775366,22.8087050174693,-16.6424241534016));
#34006=CARTESIAN_POINT('Ctrl Pts',(-26.66499058144,22.7225784674869,-16.6370856317034));
#34007=CARTESIAN_POINT('Ctrl Pts',(-26.6590567980103,22.7005623127291,-16.6357099061423));
#34008=CARTESIAN_POINT('Ctrl Pts',(-26.6500995820468,22.6686787853832,-16.633700744437));
#34009=CARTESIAN_POINT('Ctrl Pts',(-26.6472615032878,22.6587597208574,-16.633073306443));
#34010=CARTESIAN_POINT('Ctrl Pts',(-26.6420859260347,22.6409941227649,-16.6319451783293));
#34011=CARTESIAN_POINT('Ctrl Pts',(-26.639766054212,22.6331425138677,-16.6314450655755));
#34012=CARTESIAN_POINT('Ctrl Pts',(-26.6362174456555,22.6212985174817,-16.6306883133069));
#34013=CARTESIAN_POINT('Ctrl Pts',(-26.6350108118583,22.6172994978173,-16.6304323985157));
#34014=CARTESIAN_POINT('Ctrl Pts',(-26.6329144750519,22.6104003583475,-16.6299901901601));
#34015=CARTESIAN_POINT('Ctrl Pts',(-26.6320284436364,22.6074991210713,-16.6298040173237));
#34016=CARTESIAN_POINT('Ctrl Pts',(-26.6301879575527,22.6015029204434,-16.6294187943395));
#34017=CARTESIAN_POINT('Ctrl Pts',(-26.6292329312423,22.5984081371756,-16.6292197255728));
#34018=CARTESIAN_POINT('Ctrl Pts',(-26.6269102882543,22.5909216351242,-16.6287375659948));
#34019=CARTESIAN_POINT('Ctrl Pts',(-26.6255379341191,22.586531403252,-16.6284543195392));
#34020=CARTESIAN_POINT('Ctrl Pts',(-26.6204098318996,22.5702488337087,-16.6274019476845));
#34021=CARTESIAN_POINT('Ctrl Pts',(-26.6165944989754,22.5583755087048,-16.6266308612285));
#34022=CARTESIAN_POINT('Ctrl Pts',(-26.5540100184194,22.3674249943145,-16.614169571502));
#34023=CARTESIAN_POINT('Ctrl Pts',(-26.4797231918104,22.1938532985899,-16.6019506643725));
#34024=CARTESIAN_POINT('Ctrl Pts',(-26.3423136630922,21.9374880641703,-16.5825376998385));
#34025=CARTESIAN_POINT('Ctrl Pts',(-26.2896358508681,21.8495491082791,-16.5756123557096));
#34026=CARTESIAN_POINT('Ctrl Pts',(-26.2106961338803,21.7309787382728,-16.565970089807));
#34027=CARTESIAN_POINT('Ctrl Pts',(-26.1879128567065,21.6981009901301,-16.563262352275));
#34028=CARTESIAN_POINT('Ctrl Pts',(-26.1430823207508,21.6359130648195,-16.5580832208535));
#34029=CARTESIAN_POINT('Ctrl Pts',(-26.1211348805077,21.6065380639062,-16.5556112898802));
#34030=CARTESIAN_POINT('Ctrl Pts',(-26.0410196708019,21.5030414693933,-16.5468239092346));
#34031=CARTESIAN_POINT('Ctrl Pts',(-25.9801044745044,21.4310978757263,-16.5405681664569));
#34032=CARTESIAN_POINT('Ctrl Pts',(-25.8852863209428,21.3285872402985,-16.5315460945985));
#34033=CARTESIAN_POINT('Ctrl Pts',(-25.8537498930171,21.2959056416921,-16.528652325866));
#34034=CARTESIAN_POINT('Ctrl Pts',(-25.8190518514082,21.2614363695734,-16.5255918707849));
#34035=CARTESIAN_POINT('Ctrl Pts',(-25.8165683749491,21.258977280659,-16.5253734864821));
#34036=CARTESIAN_POINT('Ctrl Pts',(-25.8124580806187,21.2549205697077,-16.5250131522398));
#34037=CARTESIAN_POINT('Ctrl Pts',(-25.8108335667756,21.2533206334423,-16.5248710210871));
#34038=CARTESIAN_POINT('Ctrl Pts',(-25.8079219512546,21.2504591491101,-16.5246167896617));
#34039=CARTESIAN_POINT('Ctrl Pts',(-25.8066354889158,21.2491969563128,-16.524504638403));
#34040=CARTESIAN_POINT('Ctrl Pts',(-25.8040137942302,21.2466290334321,-16.5242764473557));
#34041=CARTESIAN_POINT('Ctrl Pts',(-25.8026784875798,21.2453233866735,-16.524160414393));
#34042=CARTESIAN_POINT('Ctrl Pts',(-25.800006808813,21.2427155901679,-16.5239286387234));
#34043=CARTESIAN_POINT('Ctrl Pts',(-25.7986704461279,21.2414134454824,-16.5238128962442));
#34044=CARTESIAN_POINT('Ctrl Pts',(-25.7948963291772,21.2377423502139,-16.5234865548486));
#34045=CARTESIAN_POINT('Ctrl Pts',(-25.7924559474699,21.235376085841,-16.5232761681639));
#34046=CARTESIAN_POINT('Ctrl Pts',(-25.7823279709486,21.2255867499938,-16.5224056083224));
#34047=CARTESIAN_POINT('Ctrl Pts',(-25.7746071077891,21.2181979674697,-16.5217480953287));
#34048=CARTESIAN_POINT('Ctrl Pts',(-25.6334098933532,21.0844129545713,-16.5098317112634));
#34049=CARTESIAN_POINT('Ctrl Pts',(-25.4893743647855,20.9696058041119,-16.4994148506551));
#34050=CARTESIAN_POINT('Ctrl Pts',(-25.2578284535008,20.8154413175926,-16.4838214781806));
#34051=CARTESIAN_POINT('Ctrl Pts',(-25.1770890224939,20.7666557597724,-16.4785742993486));
#34052=CARTESIAN_POINT('Ctrl Pts',(-24.9983566505112,20.6690953877579,-16.4671524469688));
#34053=CARTESIAN_POINT('Ctrl Pts',(-24.8997875434432,20.6216308283257,-16.4609699269727));
#34054=CARTESIAN_POINT('Ctrl Pts',(-24.7257810379265,20.5484932580268,-16.4500536522867));
#34055=CARTESIAN_POINT('Ctrl Pts',(-24.6514523432598,20.520436776313,-16.4453907653291));
#34056=CARTESIAN_POINT('Ctrl Pts',(-24.5380680548735,20.4823618413013,-16.4382322928957));
#34057=CARTESIAN_POINT('Ctrl Pts',(-24.4997342475392,20.4702822324298,-16.4358046542446));
#34058=CARTESIAN_POINT('Ctrl Pts',(-24.4539743928971,20.4567980095001,-16.4328946945276));
#34059=CARTESIAN_POINT('Ctrl Pts',(-24.4467555739866,20.4546982393341,-16.4324352849339));
#34060=CARTESIAN_POINT('Ctrl Pts',(-24.4356501635879,20.4515100632595,-16.4317279695858));
#34061=CARTESIAN_POINT('Ctrl Pts',(-24.4317687307528,20.4504036575062,-16.4314806519444));
#34062=CARTESIAN_POINT('Ctrl Pts',(-24.4249819734829,20.4484828641797,-16.43104802516));
#34063=CARTESIAN_POINT('Ctrl Pts',(-24.4220775585106,20.4476652582781,-16.4308628212446));
#34064=CARTESIAN_POINT('Ctrl Pts',(-24.4159882688092,20.4459603214166,-16.4304744022758));
#34065=CARTESIAN_POINT('Ctrl Pts',(-24.4128031698434,20.4450738106206,-16.4302711607403));
#34066=CARTESIAN_POINT('Ctrl Pts',(-24.4039522627154,20.4426250002837,-16.4297061779155));
#34067=CARTESIAN_POINT('Ctrl Pts',(-24.3982835575465,20.4410733018675,-16.4293440920044));
#34068=CARTESIAN_POINT('Ctrl Pts',(-24.3757642254869,20.434975237549,-16.4279047298507));
#34069=CARTESIAN_POINT('Ctrl Pts',(-24.35888127498,20.4305503484322,-16.4268235150889));
#34070=CARTESIAN_POINT('Ctrl Pts',(-24.0794142380463,20.359725173855,-16.4088888859524));
#34071=CARTESIAN_POINT('Ctrl Pts',(-23.8095830196128,20.3265650428403,-16.3908925750674));
#34072=CARTESIAN_POINT('Ctrl Pts',(-23.3999439815969,20.3280140542681,-16.3631738479551));
#34073=CARTESIAN_POINT('Ctrl Pts',(-23.2612066785752,20.3374859424437,-16.3537457575569));
#34074=CARTESIAN_POINT('Ctrl Pts',(-23.0393590391651,20.3671231030872,-16.3389486175802));
#34075=CARTESIAN_POINT('Ctrl Pts',(-22.955677393428,20.3816868521624,-16.3334342857079));
#34076=CARTESIAN_POINT('Ctrl Pts',(-22.863391933768,20.4015337497925,-16.3274981078645));
#34077=CARTESIAN_POINT('Ctrl Pts',(-22.8541317380503,20.403568039325,-16.326904102412));
#34078=CARTESIAN_POINT('Ctrl Pts',(-22.8425901882034,20.4061569416004,-16.3261659312334));
#34079=CARTESIAN_POINT('Ctrl Pts',(-22.8403004126517,20.4066731926616,-16.3260195893414));
#34080=CARTESIAN_POINT('Ctrl Pts',(-22.8362328753497,20.4075949274258,-16.3257598214364));
#34081=CARTESIAN_POINT('Ctrl Pts',(-22.8344548932591,20.4079994183753,-16.3256463383676));
#34082=CARTESIAN_POINT('Ctrl Pts',(-22.8310193026044,20.408784082569,-16.3254271830307));
#34083=CARTESIAN_POINT('Ctrl Pts',(-22.8293616499371,20.4091640593123,-16.3253214993992));
#34084=CARTESIAN_POINT('Ctrl Pts',(-22.8259585942386,20.4099469632174,-16.3251046565664));
#34085=CARTESIAN_POINT('Ctrl Pts',(-22.8242132301794,20.4103500325812,-16.3249935059994));
#34086=CARTESIAN_POINT('Ctrl Pts',(-22.8200135118094,20.4113235924505,-16.3247262063095));
#34087=CARTESIAN_POINT('Ctrl Pts',(-22.8175594840771,20.411895507731,-16.3245701399173));
#34088=CARTESIAN_POINT('Ctrl Pts',(-22.8086109370771,20.4139920497274,-16.3240014964818));
#34089=CARTESIAN_POINT('Ctrl Pts',(-22.8021204264702,20.4155339764382,-16.3235899132966));
#34090=CARTESIAN_POINT('Ctrl Pts',(-22.6902346679673,20.4424815583643,-16.3165090402039));
#34091=CARTESIAN_POINT('Ctrl Pts',(-22.5861694055381,20.4731726451618,-16.3101392002413));
#34092=CARTESIAN_POINT('Ctrl Pts',(-22.456434731379,20.5186649194803,-16.3022466897869));
#34093=CARTESIAN_POINT('Ctrl Pts',(-22.4291621753271,20.5286441345075,-16.3005903899509));
#34094=CARTESIAN_POINT('Ctrl Pts',(-22.3719660104479,20.5504536150014,-16.2971158519121));
#34095=CARTESIAN_POINT('Ctrl Pts',(-22.3420771812277,20.5623661469095,-16.2952996205389));
#34096=CARTESIAN_POINT('Ctrl Pts',(-22.1644578634802,20.6362594535201,-16.2844771103072));
#34097=CARTESIAN_POINT('Ctrl Pts',(-22.0213401700413,20.7087371590719,-16.2756227027085));
#34098=CARTESIAN_POINT('Ctrl Pts',(-21.7749291177407,20.8575511228047,-16.2593166869138));
#34099=CARTESIAN_POINT('Ctrl Pts',(-21.669681139088,20.9299738534172,-16.2519626370568));
#34100=CARTESIAN_POINT('Ctrl Pts',(-21.5265341488565,21.0415512642001,-16.2411732739541));
#34101=CARTESIAN_POINT('Ctrl Pts',(-21.4848953716723,21.0757187541497,-16.2379327470344));
#34102=CARTESIAN_POINT('Ctrl Pts',(-21.4379904089147,21.1162163431359,-16.2341545335701));
#34103=CARTESIAN_POINT('Ctrl Pts',(-21.431866917209,21.121543856496,-16.2336587105104));
#34104=CARTESIAN_POINT('Ctrl Pts',(-21.4226336692887,21.1296383813033,-16.2329071545356));
#34105=CARTESIAN_POINT('Ctrl Pts',(-21.4195090090389,21.1323884062438,-16.2326521313249));
#34106=CARTESIAN_POINT('Ctrl Pts',(-21.4141178385373,21.1371517617791,-16.2322109319245));
#34107=CARTESIAN_POINT('Ctrl Pts',(-21.411848819817,21.1391622559058,-16.2320248748496));
#34108=CARTESIAN_POINT('Ctrl Pts',(-21.4071569665038,21.1433313674799,-16.2316393864508));
#34109=CARTESIAN_POINT('Ctrl Pts',(-21.4047345493572,21.1454904479051,-16.2314399357565));
#34110=CARTESIAN_POINT('Ctrl Pts',(-21.3981622312779,21.1513661366627,-16.2308976505708));
#34111=CARTESIAN_POINT('Ctrl Pts',(-21.3940187138381,21.1550898400334,-16.2305545168224));
#34112=CARTESIAN_POINT('Ctrl Pts',(-21.3785165886383,21.1690941444336,-16.2292660340754));
#34113=CARTESIAN_POINT('Ctrl Pts',(-21.3672218213473,21.1794448262429,-16.2283177141028));
#34114=CARTESIAN_POINT('Ctrl Pts',(-21.1844520724328,21.3493510390126,-16.2128142848181));
#34115=CARTESIAN_POINT('Ctrl Pts',(-21.0308359506586,21.527018231633,-16.1974236057871));
#34116=CARTESIAN_POINT('Ctrl Pts',(-20.8135628732052,21.8418423436627,-16.1716383790066));
#34117=CARTESIAN_POINT('Ctrl Pts',(-20.7378146135334,21.9696421185441,-16.1615288190238));
#34118=CARTESIAN_POINT('Ctrl Pts',(-20.6316891724106,22.1806485595747,-16.1457489330931));
#34119=CARTESIAN_POINT('Ctrl Pts',(-20.5954557133736,22.2606768149133,-16.1399601878728));
#34120=CARTESIAN_POINT('Ctrl Pts',(-20.5499157020365,22.37329487001,-16.1321719124068));
#34121=CARTESIAN_POINT('Ctrl Pts',(-20.5377867580971,22.4046956298663,-16.1300378091248));
#34122=CARTESIAN_POINT('Ctrl Pts',(-20.5245556003294,22.4406143220484,-16.127643657651));
#34123=CARTESIAN_POINT('Ctrl Pts',(-20.5229690851477,22.4449499434066,-16.1273554411144));
#34124=CARTESIAN_POINT('Ctrl Pts',(-20.5207459217611,22.4510660879061,-16.1269499660584));
#34125=CARTESIAN_POINT('Ctrl Pts',(-20.5201015252244,22.452843758324,-16.1268322451754));
#34126=CARTESIAN_POINT('Ctrl Pts',(-20.5188097508751,22.4564171360536,-16.1265958742382));
#34127=CARTESIAN_POINT('Ctrl Pts',(-20.5181624023122,22.4582128558976,-16.1264772258986));
#34128=CARTESIAN_POINT('Ctrl Pts',(-20.5169209723379,22.4616661483733,-16.1262493168309));
#34129=CARTESIAN_POINT('Ctrl Pts',(-20.5163266550762,22.4633236296203,-16.1261400418453));
#34130=CARTESIAN_POINT('Ctrl Pts',(-20.5149239515028,22.4672457197641,-16.1258817346467));
#34131=CARTESIAN_POINT('Ctrl Pts',(-20.5141167393244,22.4695107518074,-16.1257327731335));
#34132=CARTESIAN_POINT('Ctrl Pts',(-20.5117226560127,22.4762523849963,-16.1252900307727));
#34133=CARTESIAN_POINT('Ctrl Pts',(-20.51014313618,22.4807316181515,-16.124996687449));
#34134=CARTESIAN_POINT('Ctrl Pts',(-20.4958001610431,22.5216942124813,-16.1223214154674));
#34135=CARTESIAN_POINT('Ctrl Pts',(-20.483683416088,22.5584029031709,-16.1199772126381));
#34136=CARTESIAN_POINT('Ctrl Pts',(-20.4696392058571,22.6036715724507,-16.1171410835519));
#34137=CARTESIAN_POINT('Ctrl Pts',(-20.467082982401,22.6120310709995,-16.1166196212295));
#34138=CARTESIAN_POINT('Ctrl Pts',(-20.4622153522642,22.6281841932491,-16.1156161847289));
#34139=CARTESIAN_POINT('Ctrl Pts',(-20.4598993627259,22.6359763502786,-16.1151340084135));
#34140=CARTESIAN_POINT('Ctrl Pts',(-20.4543113080989,22.6550412271751,-16.113958668943));
#34141=CARTESIAN_POINT('Ctrl Pts',(-20.4510712783074,22.6663232894665,-16.1132668761383));
#34142=CARTESIAN_POINT('Ctrl Pts',(-20.443329185366,22.693847862018,-16.1115876639134));
#34143=CARTESIAN_POINT('Ctrl Pts',(-20.4388927268382,22.7101086025939,-16.1106028476062));
#34144=CARTESIAN_POINT('Ctrl Pts',(-20.4191558309595,22.784750479676,-16.1061121250309));
#34145=CARTESIAN_POINT('Ctrl Pts',(-20.4053690385359,22.8435217605578,-16.1026595942019));
#34146=CARTESIAN_POINT('Ctrl Pts',(-20.3510374635455,23.1083831230778,-16.0873367906854));
#34147=CARTESIAN_POINT('Ctrl Pts',(-20.3290460777488,23.3177497492138,-16.0758257934289));
#34148=CARTESIAN_POINT('Ctrl Pts',(-20.3268123077351,23.6379526737028,-16.057568707257));
#34149=CARTESIAN_POINT('Ctrl Pts',(-20.331694738321,23.7480919561354,-16.0511785528916));
#34150=CARTESIAN_POINT('Ctrl Pts',(-20.346907018349,23.9067938168242,-16.0416797053643));
#34151=CARTESIAN_POINT('Ctrl Pts',(-20.3527307720229,23.9557132030965,-16.0387118939301));
#34152=CARTESIAN_POINT('Ctrl Pts',(-20.3607918052294,24.0123356758224,-16.0352243408427));
#34153=CARTESIAN_POINT('Ctrl Pts',(-20.3619394828733,24.0201891856069,-16.0347394469777));
#34154=CARTESIAN_POINT('Ctrl Pts',(-20.3637276934001,24.0321176919695,-16.0340011450163));
#34155=CARTESIAN_POINT('Ctrl Pts',(-20.3643470639763,24.0361958702281,-16.0337484090218));
#34156=CARTESIAN_POINT('Ctrl Pts',(-20.3654344996915,24.0432645270689,-16.0333097830818));
#34157=CARTESIAN_POINT('Ctrl Pts',(-20.3658989524952,24.04625556303,-16.0331240081208));
#34158=CARTESIAN_POINT('Ctrl Pts',(-20.3668726234891,24.0524681830509,-16.0327377742826));
#34159=CARTESIAN_POINT('Ctrl Pts',(-20.3673825196473,24.0556896560851,-16.0325372940408));
#34160=CARTESIAN_POINT('Ctrl Pts',(-20.3686363724465,24.0635342324366,-16.032048607708));
#34161=CARTESIAN_POINT('Ctrl Pts',(-20.369385514774,24.0681564894043,-16.0317602369052));
#34162=CARTESIAN_POINT('Ctrl Pts',(-20.3722543180792,24.0856161548773,-16.0306693651491));
#34163=CARTESIAN_POINT('Ctrl Pts',(-20.3744416191771,24.098442183845,-16.029864713691));
#34164=CARTESIAN_POINT('Ctrl Pts',(-20.413516903677,24.3194881486243,-16.0159394306964));
#34165=CARTESIAN_POINT('Ctrl Pts',(-20.4707245656831,24.5235508593853,-16.0021455179283));
#34166=CARTESIAN_POINT('Ctrl Pts',(-20.6245276397996,24.9181951085208,-15.9737230216388));
#34167=CARTESIAN_POINT('Ctrl Pts',(-20.7209028401736,25.1077871698904,-15.9591664840777));
#34168=CARTESIAN_POINT('Ctrl Pts',(-20.8752433936825,25.3491313138205,-15.9402919596216));
#34169=CARTESIAN_POINT('Ctrl Pts',(-20.9174324149907,25.4103329088577,-15.9354772446921));
#34170=CARTESIAN_POINT('Ctrl Pts',(-20.9662614904042,25.4761721586606,-15.93031239053));
#34171=CARTESIAN_POINT('Ctrl Pts',(-20.9708414918576,25.4823019102951,-15.9298316821384));
#34172=CARTESIAN_POINT('Ctrl Pts',(-20.9788571997769,25.4929506123127,-15.9289969324869));
#34173=CARTESIAN_POINT('Ctrl Pts',(-20.9822830717815,25.497476874078,-15.9286422288976));
#34174=CARTESIAN_POINT('Ctrl Pts',(-20.9872547942927,25.5040095727518,-15.9281304766472));
#34175=CARTESIAN_POINT('Ctrl Pts',(-20.9887910542632,25.5060232434982,-15.9279727574624));
#34176=CARTESIAN_POINT('Ctrl Pts',(-20.9914846067776,25.5095452314235,-15.9276969488652));
#34177=CARTESIAN_POINT('Ctrl Pts',(-20.9926408616912,25.5110543376741,-15.9275787856276));
#34178=CARTESIAN_POINT('Ctrl Pts',(-20.9948771583557,25.5139677356675,-15.9273506975588));
#34179=CARTESIAN_POINT('Ctrl Pts',(-20.9959570201304,25.5153721567105,-15.9272407602935));
#34180=CARTESIAN_POINT('Ctrl Pts',(-20.9985305265296,25.5187134414523,-15.9269792378122));
#34181=CARTESIAN_POINT('Ctrl Pts',(-21.0000252217931,25.5206495000266,-15.9268277275541));
#34182=CARTESIAN_POINT('Ctrl Pts',(-21.0053310469445,25.5275059128826,-15.9262912464631));
#34183=CARTESIAN_POINT('Ctrl Pts',(-21.0091542560121,25.5324169678143,-15.9259071294703));
#34184=CARTESIAN_POINT('Ctrl Pts',(-21.0616195490663,25.5994093262723,-15.9206689085217));
#34185=CARTESIAN_POINT('Ctrl Pts',(-21.1125151687427,25.6597019085795,-15.9159729156732));
#34186=CARTESIAN_POINT('Ctrl Pts',(-21.1893537875207,25.7442270375602,-15.9093153633111));
#34187=CARTESIAN_POINT('Ctrl Pts',(-21.2135601287548,25.7699903025009,-15.9072755395345));
#34188=CARTESIAN_POINT('Ctrl Pts',(-21.4289105364382,25.9917643112244,-15.8895688304469));
#34189=CARTESIAN_POINT('Ctrl Pts',(-21.6438846905835,26.163076038386,-15.8747612741233));
#34190=CARTESIAN_POINT('Ctrl Pts',(-21.9423331558195,26.3442438517148,-15.8546127577004));
#34191=CARTESIAN_POINT('Ctrl Pts',(-22.0080725960456,26.3810600756767,-15.850204687245));
#34192=CARTESIAN_POINT('Ctrl Pts',(-22.0750360164986,26.4155367751497,-15.845717117064));
#34193=CARTESIAN_POINT('Origin',(-23.5502525316942,23.5502525316942,-77.3107734492734));
#34194=CARTESIAN_POINT('',(-22.0750360145738,26.4155367741587,-14.3492876249023));
#34195=CARTESIAN_POINT('',(-22.0750361948364,26.4155368669684,-14.5938261690085));
#34196=CARTESIAN_POINT('',(-22.0750360153461,26.4155367745563,-77.3107734492734));
#34197=CARTESIAN_POINT('',(-26.7730011825842,23.5473036867677,-15.1896424574236));
#34198=CARTESIAN_POINT('Ctrl Pts',(-22.0750360145738,26.4155367741587,-14.3492876249023));
#34199=CARTESIAN_POINT('Ctrl Pts',(-22.0575688255074,26.4065436399221,-14.3505366306308));
#34200=CARTESIAN_POINT('Ctrl Pts',(-22.0401831532783,26.3973904119975,-14.3517769408737));
#34201=CARTESIAN_POINT('Ctrl Pts',(-22.0178226531192,26.3853555688787,-14.3533673775319));
#34202=CARTESIAN_POINT('Ctrl Pts',(-22.0127713311615,26.3826194082525,-14.3537263452519));
#34203=CARTESIAN_POINT('Ctrl Pts',(-22.0057073247074,26.378768566466,-14.3542278676196));
#34204=CARTESIAN_POINT('Ctrl Pts',(-22.0036885151667,26.3776652356076,-14.3543711423095));
#34205=CARTESIAN_POINT('Ctrl Pts',(-21.9999975015453,26.3756428666488,-14.3546329909806));
#34206=CARTESIAN_POINT('Ctrl Pts',(-21.9983249299616,26.3747245040096,-14.3547516084697));
#34207=CARTESIAN_POINT('Ctrl Pts',(-21.9949300319399,26.3728565337436,-14.3549922924005));
#34208=CARTESIAN_POINT('Ctrl Pts',(-21.9932077586214,26.3719068346384,-14.3551143527132));
#34209=CARTESIAN_POINT('Ctrl Pts',(-21.9889829197636,26.3695721202513,-14.3554136744765));
#34210=CARTESIAN_POINT('Ctrl Pts',(-21.9864813205783,26.3681853454775,-14.3555908222648));
#34211=CARTESIAN_POINT('Ctrl Pts',(-21.977318120931,26.3630897175642,-14.3562394012561));
#34212=CARTESIAN_POINT('Ctrl Pts',(-21.9706677733736,26.3593605198019,-14.3567095323155));
#34213=CARTESIAN_POINT('Ctrl Pts',(-21.8159756742526,26.2718935226117,-14.3676329349495));
#34214=CARTESIAN_POINT('Ctrl Pts',(-21.674755321772,26.1765759007306,-14.3773499617286));
#34215=CARTESIAN_POINT('Ctrl Pts',(-21.3844110429276,25.9451852310465,-14.3982293484068));
#34216=CARTESIAN_POINT('Ctrl Pts',(-21.2392047384932,25.8053863497996,-14.4093053138431));
#34217=CARTESIAN_POINT('Ctrl Pts',(-21.0831217699524,25.6240978686232,-14.4230365260751));
#34218=CARTESIAN_POINT('Ctrl Pts',(-21.0587817396057,25.5947920468528,-14.4252375569533));
#34219=CARTESIAN_POINT('Ctrl Pts',(-20.9740065710603,25.488958874302,-14.4331351199572));
#34220=CARTESIAN_POINT('Ctrl Pts',(-20.916536378735,25.4101347438325,-14.4389264458014));
#34221=CARTESIAN_POINT('Ctrl Pts',(-20.8575886998007,25.3210619166707,-14.445427986792));
#34222=CARTESIAN_POINT('Ctrl Pts',(-20.8524799694093,25.3132691478456,-14.4459964242809));
#34223=CARTESIAN_POINT('Ctrl Pts',(-20.8449446023952,25.3016653845281,-14.4468423518024));
#34224=CARTESIAN_POINT('Ctrl Pts',(-20.8424920363326,25.2978712180274,-14.4471188718738));
#34225=CARTESIAN_POINT('Ctrl Pts',(-20.8383070689721,25.2913670354288,-14.447592769086));
#34226=CARTESIAN_POINT('Ctrl Pts',(-20.8365707266426,25.2886595521338,-14.4477899989938));
#34227=CARTESIAN_POINT('Ctrl Pts',(-20.8332005258119,25.2833870356314,-14.4481740094175));
#34228=CARTESIAN_POINT('Ctrl Pts',(-20.8315662389448,25.2808222797617,-14.4483607736759));
#34229=CARTESIAN_POINT('Ctrl Pts',(-20.8276658760257,25.2746821137794,-14.4488078201755));
#34230=CARTESIAN_POINT('Ctrl Pts',(-20.825403213664,25.2711045517557,-14.4490682288033));
#34231=CARTESIAN_POINT('Ctrl Pts',(-20.8189185811264,25.2608066527492,-14.4498176336531));
#34232=CARTESIAN_POINT('Ctrl Pts',(-20.8147144007027,25.254075199306,-14.4503072876308));
#34233=CARTESIAN_POINT('Ctrl Pts',(-20.7840685504616,25.2046012934978,-14.4539046363932));
#34234=CARTESIAN_POINT('Ctrl Pts',(-20.7586063758491,25.1612630602446,-14.4570481432129));
#34235=CARTESIAN_POINT('Ctrl Pts',(-20.6782440204722,25.016851344877,-14.4675059279114));
#34236=CARTESIAN_POINT('Ctrl Pts',(-20.6277447226589,24.9134429099686,-14.4749714358207));
#34237=CARTESIAN_POINT('Ctrl Pts',(-20.500943585716,24.6141813334663,-14.4964816459474));
#34238=CARTESIAN_POINT('Ctrl Pts',(-20.4381078469019,24.4132552915898,-14.5108462901237));
#34239=CARTESIAN_POINT('Ctrl Pts',(-20.3781682190555,24.1256013568599,-14.5305701779059));
#34240=CARTESIAN_POINT('Ctrl Pts',(-20.3642748138311,24.0428914228154,-14.5361414546074));
#34241=CARTESIAN_POINT('Ctrl Pts',(-20.3532218357711,23.9566048540769,-14.5417930348087));
#34242=CARTESIAN_POINT('Ctrl Pts',(-20.3528262698671,23.9534804832394,-14.5419974558662));
#34243=CARTESIAN_POINT('Ctrl Pts',(-20.3518319846269,23.9455336732009,-14.5425168357428));
#34244=CARTESIAN_POINT('Ctrl Pts',(-20.3512395895143,23.9407104334669,-14.5428315410619));
#34245=CARTESIAN_POINT('Ctrl Pts',(-20.3504590504145,23.9342343110051,-14.5432533697134));
#34246=CARTESIAN_POINT('Ctrl Pts',(-20.3502612766049,23.9325826208282,-14.5433608910492));
#34247=CARTESIAN_POINT('Ctrl Pts',(-20.3492955422134,23.9244641338245,-14.5438890737585));
#34248=CARTESIAN_POINT('Ctrl Pts',(-20.3485458992505,23.9179951221678,-14.5443089680674));
#34249=CARTESIAN_POINT('Ctrl Pts',(-20.3435190506629,23.87343535685,-14.5471943710217));
#34250=CARTESIAN_POINT('Ctrl Pts',(-20.3399018515944,23.835271113821,-14.5496309223314));
#34251=CARTESIAN_POINT('Ctrl Pts',(-20.3365632585357,23.7918027492416,-14.5523598351374));
#34252=CARTESIAN_POINT('Ctrl Pts',(-20.3361731376469,23.786555095597,-14.5526885131588));
#34253=CARTESIAN_POINT('Ctrl Pts',(-20.3356210138338,23.7788738670702,-14.5531684700172));
#34254=CARTESIAN_POINT('Ctrl Pts',(-20.3354489202794,23.7764410608908,-14.5533203145268));
#34255=CARTESIAN_POINT('Ctrl Pts',(-20.3351487453475,23.772128075526,-14.5535892106962));
#34256=CARTESIAN_POINT('Ctrl Pts',(-20.3350195514235,23.7702479784305,-14.5537063254471));
#34257=CARTESIAN_POINT('Ctrl Pts',(-20.3347528056066,23.7663157266867,-14.5539510599603));
#34258=CARTESIAN_POINT('Ctrl Pts',(-20.3346155693772,23.7642635579001,-14.5540786614417));
#34259=CARTESIAN_POINT('Ctrl Pts',(-20.3342658271957,23.7589573775578,-14.5544082842872));
#34260=CARTESIAN_POINT('Ctrl Pts',(-20.3340562946956,23.7557031621097,-14.5546101372365));
#34261=CARTESIAN_POINT('Ctrl Pts',(-20.3331829432767,23.7418104686691,-14.5554706130383));
#34262=CARTESIAN_POINT('Ctrl Pts',(-20.3325669569016,23.7311688914989,-14.5561265645515));
#34263=CARTESIAN_POINT('Ctrl Pts',(-20.3311027193244,23.7034938316689,-14.5578247101151));
#34264=CARTESIAN_POINT('Ctrl Pts',(-20.3303368446282,23.6864560824771,-14.5588625136608));
#34265=CARTESIAN_POINT('Ctrl Pts',(-20.3277896372984,23.6176125813417,-14.5630279636414));
#34266=CARTESIAN_POINT('Ctrl Pts',(-20.3271229468472,23.5657706382902,-14.5661008593813));
#34267=CARTESIAN_POINT('Ctrl Pts',(-20.3289532862687,23.4033727761203,-14.575589149138));
#34268=CARTESIAN_POINT('Ctrl Pts',(-20.3358882773262,23.2929427909179,-14.5818426856793));
#34269=CARTESIAN_POINT('Ctrl Pts',(-20.3649018457246,23.0399419932142,-14.5961281455535));
#34270=CARTESIAN_POINT('Ctrl Pts',(-20.3908966906889,22.8980669791499,-14.604113157778));
#34271=CARTESIAN_POINT('Ctrl Pts',(-20.4698707194228,22.5865015144479,-14.6223140775673));
#34272=CARTESIAN_POINT('Ctrl Pts',(-20.5275526817546,22.4185106500106,-14.6325978444968));
#34273=CARTESIAN_POINT('Ctrl Pts',(-20.6033762912805,22.2455798925902,-14.6440802920628));
#34274=CARTESIAN_POINT('Ctrl Pts',(-20.6080587087546,22.23505453351,-14.6447827381274));
#34275=CARTESIAN_POINT('Ctrl Pts',(-20.6146265479053,22.2205016459751,-14.6457590134565));
#34276=CARTESIAN_POINT('Ctrl Pts',(-20.6164640636208,22.2164524870682,-14.6460311927266));
#34277=CARTESIAN_POINT('Ctrl Pts',(-20.6196372377056,22.209498346903,-14.6464995802726));
#34278=CARTESIAN_POINT('Ctrl Pts',(-20.6209688535655,22.2065915185166,-14.6466956488549));
#34279=CARTESIAN_POINT('Ctrl Pts',(-20.623720428987,22.2006085440789,-14.6470997915825));
#34280=CARTESIAN_POINT('Ctrl Pts',(-20.6251409173961,22.197532647445,-14.6473078838005));
#34281=CARTESIAN_POINT('Ctrl Pts',(-20.6284488043302,22.1903993904504,-14.647791210669));
#34282=CARTESIAN_POINT('Ctrl Pts',(-20.6303398049179,22.1863437170456,-14.6480665698329));
#34283=CARTESIAN_POINT('Ctrl Pts',(-20.6362476362963,22.1737416497778,-14.6489239353258));
#34284=CARTESIAN_POINT('Ctrl Pts',(-20.6402935611782,22.1652090214372,-14.6495069508751));
#34285=CARTESIAN_POINT('Ctrl Pts',(-20.6958608318373,22.0493390258184,-14.6574586241757));
#34286=CARTESIAN_POINT('Ctrl Pts',(-20.7532480299174,21.9449322694041,-14.6650332158471));
#34287=CARTESIAN_POINT('Ctrl Pts',(-20.9283046359657,21.664442208574,-14.6865859010637));
#34288=CARTESIAN_POINT('Ctrl Pts',(-21.0577327806941,21.4964226521994,-14.7009457752117));
#34289=CARTESIAN_POINT('Ctrl Pts',(-21.3063803895804,21.2320482366041,-14.7254769411422));
#34290=CARTESIAN_POINT('Ctrl Pts',(-21.4177441317677,21.1292091593249,-14.7356337009553));
#34291=CARTESIAN_POINT('Ctrl Pts',(-21.5376361749517,21.0332110728419,-14.7454597151126));
#34292=CARTESIAN_POINT('Ctrl Pts',(-21.5393374965901,21.0318516448897,-14.7455989358607));
#34293=CARTESIAN_POINT('Ctrl Pts',(-21.5629531434609,21.0130209326772,-14.7475284347227));
#34294=CARTESIAN_POINT('Ctrl Pts',(-21.5850940099488,20.9958337796463,-14.7493017469318));
#34295=CARTESIAN_POINT('Ctrl Pts',(-21.6112322966511,20.976084612155,-14.7513511528556));
#34296=CARTESIAN_POINT('Ctrl Pts',(-21.6150137202537,20.9732405617439,-14.7516465763119));
#34297=CARTESIAN_POINT('Ctrl Pts',(-21.6207170836991,20.9689706323066,-14.7520905343305));
#34298=CARTESIAN_POINT('Ctrl Pts',(-21.6226343494491,20.9675385651963,-14.7522395028464));
#34299=CARTESIAN_POINT('Ctrl Pts',(-21.6260552883029,20.9649892878113,-14.7525048132422));
#34300=CARTESIAN_POINT('Ctrl Pts',(-21.6275583389808,20.9638712541134,-14.752621213326));
#34301=CARTESIAN_POINT('Ctrl Pts',(-21.6307506753295,20.961500977828,-14.7528680773018));
#34302=CARTESIAN_POINT('Ctrl Pts',(-21.6324402075769,20.9602490811644,-14.7529985166548));
#34303=CARTESIAN_POINT('Ctrl Pts',(-21.6358869016775,20.9577003979183,-14.7532641865188));
#34304=CARTESIAN_POINT('Ctrl Pts',(-21.637644159214,20.9564037417062,-14.7533994078373));
#34305=CARTESIAN_POINT('Ctrl Pts',(-21.6454429721302,20.950661338984,-14.7539985268956));
#34306=CARTESIAN_POINT('Ctrl Pts',(-21.6514987850783,20.9462348589824,-14.7544610842294));
#34307=CARTESIAN_POINT('Ctrl Pts',(-21.6663654646946,20.9354475351625,-14.7555902850245));
#34308=CARTESIAN_POINT('Ctrl Pts',(-21.675193226777,20.9291099827602,-14.7562553692522));
#34309=CARTESIAN_POINT('Ctrl Pts',(-21.7088209878239,20.9052250527912,-14.758769053955));
#34310=CARTESIAN_POINT('Ctrl Pts',(-21.733837475804,20.8879833888735,-14.7605983562596));
#34311=CARTESIAN_POINT('Ctrl Pts',(-21.8281348066066,20.8249406155197,-14.7673583511184));
#34312=CARTESIAN_POINT('Ctrl Pts',(-21.8989383414206,20.7814661488401,-14.7721660975756));
#34313=CARTESIAN_POINT('Ctrl Pts',(-22.0862793777882,20.6761819879954,-14.7844173473697));
#34314=CARTESIAN_POINT('Ctrl Pts',(-22.2050705579157,20.6187022788282,-14.7917421975329));
#34315=CARTESIAN_POINT('Ctrl Pts',(-22.552871131831,20.4760169153364,-14.8127664670626));
#34316=CARTESIAN_POINT('Ctrl Pts',(-22.7884438548675,20.409342345846,-14.8265787742771));
#34317=CARTESIAN_POINT('Ctrl Pts',(-23.0441168838522,20.3674596182057,-14.8422973047826));
#34318=CARTESIAN_POINT('Ctrl Pts',(-23.0589842438616,20.3651309513571,-14.843213559513));
#34319=CARTESIAN_POINT('Ctrl Pts',(-23.0793359235312,20.3620891597868,-14.8444710154158));
#34320=CARTESIAN_POINT('Ctrl Pts',(-23.0848067409135,20.3612858725619,-14.8448093537062));
#34321=CARTESIAN_POINT('Ctrl Pts',(-23.0934830818958,20.3600347165424,-14.8453464456185));
#34322=CARTESIAN_POINT('Ctrl Pts',(-23.0966872768557,20.3595775877582,-14.845544905345));
#34323=CARTESIAN_POINT('Ctrl Pts',(-23.1028963632434,20.3587013060153,-14.8459296962322));
#34324=CARTESIAN_POINT('Ctrl Pts',(-23.1059011699012,20.3582815677351,-14.8461160086317));
#34325=CARTESIAN_POINT('Ctrl Pts',(-23.1130487765332,20.3572934143711,-14.8465594292215));
#34326=CARTESIAN_POINT('Ctrl Pts',(-23.1171920912025,20.3567288190781,-14.8468166581291));
#34327=CARTESIAN_POINT('Ctrl Pts',(-23.1257733488591,20.3555764876093,-14.847349799984));
#34328=CARTESIAN_POINT('Ctrl Pts',(-23.1302114388364,20.3549899316414,-14.8476257497697));
#34329=CARTESIAN_POINT('Ctrl Pts',(-23.1553950791224,20.3517149344969,-14.8491928551748));
#34330=CARTESIAN_POINT('Ctrl Pts',(-23.1761648081041,20.3492193374951,-14.8504900993998));
#34331=CARTESIAN_POINT('Ctrl Pts',(-23.311918586412,20.3342470239319,-14.8590018759428));
#34332=CARTESIAN_POINT('Ctrl Pts',(-23.4274660116811,20.3277670725905,-14.866404800644));
#34333=CARTESIAN_POINT('Ctrl Pts',(-23.5684729234957,20.3274541636857,-14.8756362961598));
#34334=CARTESIAN_POINT('Ctrl Pts',(-23.5938442036817,20.3276974861467,-14.8773048826949));
#34335=CARTESIAN_POINT('Ctrl Pts',(-23.7726234968472,20.3315236908059,-14.8891137194571));
#34336=CARTESIAN_POINT('Ctrl Pts',(-23.9255973301185,20.3457597105112,-14.899496897803));
#34337=CARTESIAN_POINT('Ctrl Pts',(-24.2679048778954,20.4024672787699,-14.9229802326792));
#34338=CARTESIAN_POINT('Ctrl Pts',(-24.4556342924474,20.4512398190323,-14.9360400281714));
#34339=CARTESIAN_POINT('Ctrl Pts',(-24.6485254144695,20.5203940579723,-14.9489512266214));
#34340=CARTESIAN_POINT('Ctrl Pts',(-24.6591609075802,20.5242703905047,-14.9496613496025));
#34341=CARTESIAN_POINT('Ctrl Pts',(-24.6730366985582,20.5294107005456,-14.9505853057575));
#34342=CARTESIAN_POINT('Ctrl Pts',(-24.6762955155689,20.5306239364997,-14.9508021205004));
#34343=CARTESIAN_POINT('Ctrl Pts',(-24.6813146332027,20.532501775705,-14.9511357630521));
#34344=CARTESIAN_POINT('Ctrl Pts',(-24.683076313157,20.5331626452412,-14.951252814816));
#34345=CARTESIAN_POINT('Ctrl Pts',(-24.6865834323999,20.5344817966302,-14.9514857287252));
#34346=CARTESIAN_POINT('Ctrl Pts',(-24.6883288685655,20.53514004725,-14.9516015913762));
#34347=CARTESIAN_POINT('Ctrl Pts',(-24.69222834417,20.5366145122505,-14.9518603180991));
#34348=CARTESIAN_POINT('Ctrl Pts',(-24.6943820756408,20.5374315188784,-14.952003133377));
#34349=CARTESIAN_POINT('Ctrl Pts',(-24.698838934613,20.5391276729787,-14.9522985024685));
#34350=CARTESIAN_POINT('Ctrl Pts',(-24.7011419341183,20.5400071557773,-14.9524510359999));
#34351=CARTESIAN_POINT('Ctrl Pts',(-24.7138351372967,20.544871205589,-14.9532912381569));
#34352=CARTESIAN_POINT('Ctrl Pts',(-24.7242058289423,20.5489069901411,-14.9539758537043));
#34353=CARTESIAN_POINT('Ctrl Pts',(-24.7513187280967,20.5596200853037,-14.9557613544173));
#34354=CARTESIAN_POINT('Ctrl Pts',(-24.7680264403715,20.5663843746866,-14.9568572716985));
#34355=CARTESIAN_POINT('Ctrl Pts',(-24.8370256988262,20.5949955278656,-14.961368550071));
#34356=CARTESIAN_POINT('Ctrl Pts',(-24.8887962148524,20.6180808486393,-14.9647184312394));
#34357=CARTESIAN_POINT('Ctrl Pts',(-25.0121590636445,20.6770392084254,-14.9726779890572));
#34358=CARTESIAN_POINT('Ctrl Pts',(-25.083076828445,20.7142383302666,-14.9772349529812));
#34359=CARTESIAN_POINT('Ctrl Pts',(-25.216444826549,20.7906609473234,-14.9859011986569));
#34360=CARTESIAN_POINT('Ctrl Pts',(-25.2790773712428,20.8294608307051,-14.9900145213348));
#34361=CARTESIAN_POINT('Ctrl Pts',(-25.5607806434269,21.0176296074321,-15.0089432124281));
#34362=CARTESIAN_POINT('Ctrl Pts',(-25.7621869099377,21.1914981656296,-15.0238165702641));
#34363=CARTESIAN_POINT('Ctrl Pts',(-25.9512201375177,21.4004267992605,-15.0408932231552));
#34364=CARTESIAN_POINT('Ctrl Pts',(-25.9623213938666,21.4128896912224,-15.0419087764182));
#34365=CARTESIAN_POINT('Ctrl Pts',(-25.9771297591106,21.4297766926449,-15.0432809342589));
#34366=CARTESIAN_POINT('Ctrl Pts',(-25.9809226566522,21.4341255024506,-15.043633953751));
#34367=CARTESIAN_POINT('Ctrl Pts',(-25.9868561499726,21.4409656477735,-15.0441886815578));
#34368=CARTESIAN_POINT('Ctrl Pts',(-25.9890046645673,21.4434501238814,-15.0443900607696));
#34369=CARTESIAN_POINT('Ctrl Pts',(-25.9931220935282,21.4482261298337,-15.0447769733547));
#34370=CARTESIAN_POINT('Ctrl Pts',(-25.9950915921741,21.4505171534841,-15.0449624822638));
#34371=CARTESIAN_POINT('Ctrl Pts',(-25.9997109128501,21.4559058987425,-15.0453986087899));
#34372=CARTESIAN_POINT('Ctrl Pts',(-26.0023580803015,21.4590058800009,-15.0456493355794));
#34373=CARTESIAN_POINT('Ctrl Pts',(-26.0078056071717,21.4654098033826,-15.0461669530468));
#34374=CARTESIAN_POINT('Ctrl Pts',(-26.0106052009037,21.4687143832562,-15.0464338745385));
#34375=CARTESIAN_POINT('Ctrl Pts',(-26.0178021896918,21.4772443576292,-15.0471224065906));
#34376=CARTESIAN_POINT('Ctrl Pts',(-26.0221896347545,21.4824780851489,-15.0475444241729));
#34377=CARTESIAN_POINT('Ctrl Pts',(-26.0620951948564,21.5303894381937,-15.0514037529148));
#34378=CARTESIAN_POINT('Ctrl Pts',(-26.0965195771706,21.5739620689928,-15.0548852025836));
#34379=CARTESIAN_POINT('Ctrl Pts',(-26.2147742025962,21.7318640729124,-15.06741337013));
#34380=CARTESIAN_POINT('Ctrl Pts',(-26.2921592082476,21.8507964276416,-15.0767000472682));
#34381=CARTESIAN_POINT('Ctrl Pts',(-26.3856244079427,22.0175338694134,-15.0894727940733));
#34382=CARTESIAN_POINT('Ctrl Pts',(-26.4087952500272,22.0611946108251,-15.0927948322467));
#34383=CARTESIAN_POINT('Ctrl Pts',(-26.4418197668885,22.1270364473578,-15.0977634676192));
#34384=CARTESIAN_POINT('Ctrl Pts',(-26.4524422547958,22.1488247255272,-15.0994010956555));
#34385=CARTESIAN_POINT('Ctrl Pts',(-26.4750002078681,22.1964510172113,-15.1029647924168));
#34386=CARTESIAN_POINT('Ctrl Pts',(-26.4868412768271,22.2223315836779,-15.1048912881772));
#34387=CARTESIAN_POINT('Ctrl Pts',(-26.5799095072105,22.433081896117,-15.1204865646759));
#34388=CARTESIAN_POINT('Ctrl Pts',(-26.6439502866254,22.6250792042164,-15.1341522072137));
#34389=CARTESIAN_POINT('Ctrl Pts',(-26.6923899224194,22.8338431984258,-15.1476683709772));
#34390=CARTESIAN_POINT('Ctrl Pts',(-26.6951090005671,22.8458751350598,-15.1484426567889));
#34391=CARTESIAN_POINT('Ctrl Pts',(-26.6985314585964,22.8614344926445,-15.1494376059124));
#34392=CARTESIAN_POINT('Ctrl Pts',(-26.6992980621516,22.8649476798918,-15.1496618417252));
#34393=CARTESIAN_POINT('Ctrl Pts',(-26.7004618933235,22.8703244685306,-15.150004380943));
#34394=CARTESIAN_POINT('Ctrl Pts',(-26.7008633475779,22.8721871365773,-15.1501229277464));
#34395=CARTESIAN_POINT('Ctrl Pts',(-26.7016150688771,22.8756900551035,-15.1503456422033));
#34396=CARTESIAN_POINT('Ctrl Pts',(-26.7019657060022,22.8773302163331,-15.1504498308238));
#34397=CARTESIAN_POINT('Ctrl Pts',(-26.7027704139927,22.8811087928533,-15.150689646411));
#34398=CARTESIAN_POINT('Ctrl Pts',(-26.7032235887357,22.8832473930572,-15.1508252209289));
#34399=CARTESIAN_POINT('Ctrl Pts',(-26.7041493730521,22.8876383355476,-15.151103262638));
#34400=CARTESIAN_POINT('Ctrl Pts',(-26.7046217469071,22.8898907270308,-15.1512457161832));
#34401=CARTESIAN_POINT('Ctrl Pts',(-26.7058157791786,22.8956146730001,-15.1516072983909));
#34402=CARTESIAN_POINT('Ctrl Pts',(-26.7065341241278,22.8990869272138,-15.1518262380448));
#34403=CARTESIAN_POINT('Ctrl Pts',(-26.7085761166034,22.9090400483051,-15.1524526865943));
#34404=CARTESIAN_POINT('Ctrl Pts',(-26.7098855534321,22.9155238608583,-15.1528593980918));
#34405=CARTESIAN_POINT('Ctrl Pts',(-26.7520963747704,23.1279028300848,-15.1661375867121));
#34406=CARTESIAN_POINT('Ctrl Pts',(-26.7728090541682,23.3373294056183,-15.1779030483283));
#34407=CARTESIAN_POINT('Ctrl Pts',(-26.7730011825842,23.5473036867677,-15.1896424574236));
#34408=CARTESIAN_POINT('Ctrl Pts',(-26.7730011815105,23.5473025134888,-15.189642391827));
#34409=CARTESIAN_POINT('Ctrl Pts',(-26.7731220480874,23.6793432570931,-15.1970246309133));
#34410=CARTESIAN_POINT('Ctrl Pts',(-26.7651279187396,23.8112675563302,-15.2043751941072));
#34411=CARTESIAN_POINT('Ctrl Pts',(-26.7350653072654,24.0565379137957,-15.2184371318526));
#34412=CARTESIAN_POINT('Ctrl Pts',(-26.7149616201925,24.1699055028723,-15.2250978832352));
#34413=CARTESIAN_POINT('Ctrl Pts',(-26.6812839765029,24.3143648265673,-15.2339301582693));
#34414=CARTESIAN_POINT('Ctrl Pts',(-26.6732251997283,24.346661408296,-15.2359270959144));
#34415=CARTESIAN_POINT('Ctrl Pts',(-26.6611527625449,24.3920388695957,-15.2387668684762));
#34416=CARTESIAN_POINT('Ctrl Pts',(-26.6575536823376,24.4052285753785,-15.239596377073));
#34417=CARTESIAN_POINT('Ctrl Pts',(-26.6519660228538,24.425204519791,-15.2408590325723));
#34418=CARTESIAN_POINT('Ctrl Pts',(-26.650038824424,24.4320078837442,-15.241290187561));
#34419=CARTESIAN_POINT('Ctrl Pts',(-26.646867091773,24.4430657698963,-15.2419928163983));
#34420=CARTESIAN_POINT('Ctrl Pts',(-26.6456361352801,24.4473241890011,-15.2422638474578));
#34421=CARTESIAN_POINT('Ctrl Pts',(-26.6432357776294,24.455564314657,-15.2427891696531));
#34422=CARTESIAN_POINT('Ctrl Pts',(-26.6420674632112,24.4595463307494,-15.243043424863));
#34423=CARTESIAN_POINT('Ctrl Pts',(-26.6399511510272,24.4667082122633,-15.243501432421));
#34424=CARTESIAN_POINT('Ctrl Pts',(-26.639005925742,24.4698888964497,-15.2437050937192));
#34425=CARTESIAN_POINT('Ctrl Pts',(-26.6371054303765,24.4762480823514,-15.2441127876199));
#34426=CARTESIAN_POINT('Ctrl Pts',(-26.6361501590587,24.4794265795647,-15.2443168200571));
#34427=CARTESIAN_POINT('Ctrl Pts',(-26.6334711232074,24.4882908994902,-15.2448865508614));
#34428=CARTESIAN_POINT('Ctrl Pts',(-26.6317365492648,24.4939734179788,-15.2452526036811));
#34429=CARTESIAN_POINT('Ctrl Pts',(-26.6247045969124,24.5167842186546,-15.2467253527325));
#34430=CARTESIAN_POINT('Ctrl Pts',(-26.6192801210261,24.5338727013903,-15.2478362215902));
#34431=CARTESIAN_POINT('Ctrl Pts',(-26.5278060646413,24.8139144447451,-15.2661680402064));
#34432=CARTESIAN_POINT('Ctrl Pts',(-26.4084081479474,25.0646981230958,-15.2845861006355));
#34433=CARTESIAN_POINT('Ctrl Pts',(-26.2363188052158,25.3314996010499,-15.3060742672728));
#34434=CARTESIAN_POINT('Ctrl Pts',(-26.2134777109189,25.3654728514333,-15.3088462201104));
#34435=CARTESIAN_POINT('Ctrl Pts',(-26.1681622694999,25.4301766609059,-15.3141862757685));
#34436=CARTESIAN_POINT('Ctrl Pts',(-26.1457780977653,25.4609626710608,-15.3167546240849));
#34437=CARTESIAN_POINT('Ctrl Pts',(-26.0640199570113,25.5693197165789,-15.3258783293613));
#34438=CARTESIAN_POINT('Ctrl Pts',(-26.0016666703096,25.6445855410796,-15.3323740859227));
#34439=CARTESIAN_POINT('Ctrl Pts',(-25.9050914751152,25.7509257930706,-15.341663617091));
#34440=CARTESIAN_POINT('Ctrl Pts',(-25.8734710729006,25.7842814948884,-15.3445947125887));
#34441=CARTESIAN_POINT('Ctrl Pts',(-25.838409605783,25.8197172051514,-15.3477164718293));
#34442=CARTESIAN_POINT('Ctrl Pts',(-25.8356681104533,25.8224779458012,-15.3479597360686));
#34443=CARTESIAN_POINT('Ctrl Pts',(-25.8311948278581,25.8269663450178,-15.3483553097152));
#34444=CARTESIAN_POINT('Ctrl Pts',(-25.8294660713694,25.8286969981809,-15.3485078548546));
#34445=CARTESIAN_POINT('Ctrl Pts',(-25.8261152566336,25.8320438593307,-15.3488028901907));
#34446=CARTESIAN_POINT('Ctrl Pts',(-25.8244934437939,25.833660309437,-15.3489453996436));
#34447=CARTESIAN_POINT('Ctrl Pts',(-25.8215478010534,25.8365899606117,-15.3492037079574));
#34448=CARTESIAN_POINT('Ctrl Pts',(-25.8202245586377,25.8379037368452,-15.3493195528149));
#34449=CARTESIAN_POINT('Ctrl Pts',(-25.8175580449862,25.8405465832599,-15.3495526086458));
#34450=CARTESIAN_POINT('Ctrl Pts',(-25.8162147504733,25.84187561509,-15.3496698167091));
#34451=CARTESIAN_POINT('Ctrl Pts',(-25.8123676828936,25.8456751458137,-15.3500049285637));
#34452=CARTESIAN_POINT('Ctrl Pts',(-25.8098610231963,25.8481427379724,-15.3502226010809));
#34453=CARTESIAN_POINT('Ctrl Pts',(-25.7990309814348,25.8587691312998,-15.3511601614588));
#34454=CARTESIAN_POINT('Ctrl Pts',(-25.7906672773983,25.8668869835887,-15.3518768523136));
#34455=CARTESIAN_POINT('Ctrl Pts',(-25.6464820729941,26.0053226680869,-15.3641105584333));
#34456=CARTESIAN_POINT('Ctrl Pts',(-25.4995212726199,26.1235620252855,-15.3747503598337));
#34457=CARTESIAN_POINT('Ctrl Pts',(-25.2785814003165,26.2714685859045,-15.3896428622088));
#34458=CARTESIAN_POINT('Ctrl Pts',(-25.212569152684,26.3122881902462,-15.3939661692397));
#34459=CARTESIAN_POINT('Ctrl Pts',(-25.0756198261285,26.3902832227929,-15.4027931730439));
#34460=CARTESIAN_POINT('Ctrl Pts',(-25.0046429880872,26.4272765876484,-15.4072952460173));
#34461=CARTESIAN_POINT('Ctrl Pts',(-24.8329019432875,26.5088080197654,-15.4181349733544));
#34462=CARTESIAN_POINT('Ctrl Pts',(-24.7310929245895,26.5508945591447,-15.4245205646822));
#34463=CARTESIAN_POINT('Ctrl Pts',(-24.5967800033113,26.5985223569168,-15.4330112964077));
#34464=CARTESIAN_POINT('Ctrl Pts',(-24.5660625013207,26.6088958040356,-15.434957216392));
#34465=CARTESIAN_POINT('Ctrl Pts',(-24.5159258259378,26.624988648344,-15.4381424830605));
#34466=CARTESIAN_POINT('Ctrl Pts',(-24.4965996383479,26.6309917648829,-15.4393724888845));
#34467=CARTESIAN_POINT('Ctrl Pts',(-24.4729722702765,26.6380876152972,-15.4408792779505));
#34468=CARTESIAN_POINT('Ctrl Pts',(-24.468723398956,26.6393540977132,-15.4411503604168));
#34469=CARTESIAN_POINT('Ctrl Pts',(-24.4604919554392,26.6417892014652,-15.4416757712926));
#34470=CARTESIAN_POINT('Ctrl Pts',(-24.45650971057,26.6429589054967,-15.4419300637408));
#34471=CARTESIAN_POINT('Ctrl Pts',(-24.4493397089256,26.645049911304,-15.4423881116874));
#34472=CARTESIAN_POINT('Ctrl Pts',(-24.446152762575,26.645973990301,-15.4425917760666));
#34473=CARTESIAN_POINT('Ctrl Pts',(-24.4393088061563,26.6479469932796,-15.443029296651));
#34474=CARTESIAN_POINT('Ctrl Pts',(-24.4356513574372,26.6489943659993,-15.4432632031684));
#34475=CARTESIAN_POINT('Ctrl Pts',(-24.4257755539346,26.6518035585283,-15.4438950506039));
#34476=CARTESIAN_POINT('Ctrl Pts',(-24.4195537639769,26.653553145735,-15.4442933898549));
#34477=CARTESIAN_POINT('Ctrl Pts',(-24.3985860303906,26.6593813350175,-15.4456367579802));
#34478=CARTESIAN_POINT('Ctrl Pts',(-24.3838164902552,26.6633735949777,-15.4465845915601));
#34479=CARTESIAN_POINT('Ctrl Pts',(-24.1126700816536,26.7345975598202,-15.4640158352573));
#34480=CARTESIAN_POINT('Ctrl Pts',(-23.8490505375573,26.7700392607985,-15.4815905805253));
#34481=CARTESIAN_POINT('Ctrl Pts',(-23.440999015051,26.7743292555715,-15.509192847489));
#34482=CARTESIAN_POINT('Ctrl Pts',(-23.2979191699941,26.7662963723533,-15.5189181716028));
#34483=CARTESIAN_POINT('Ctrl Pts',(-23.0680289325428,26.7379486492674,-15.5342477704093));
#34484=CARTESIAN_POINT('Ctrl Pts',(-22.9806882689219,26.7235073268375,-15.5399989779649));
#34485=CARTESIAN_POINT('Ctrl Pts',(-22.885537460668,26.7037183922766,-15.5461058474224));
#34486=CARTESIAN_POINT('Ctrl Pts',(-22.8770376595901,26.7019147597314,-15.5466499620324));
#34487=CARTESIAN_POINT('Ctrl Pts',(-22.866311974197,26.6995934305078,-15.5473346929052));
#34488=CARTESIAN_POINT('Ctrl Pts',(-22.864079313774,26.6991077360846,-15.5474771239213));
#34489=CARTESIAN_POINT('Ctrl Pts',(-22.8597230375646,26.6981552156827,-15.5477548265462));
#34490=CARTESIAN_POINT('Ctrl Pts',(-22.8575993746171,26.697688614315,-15.5478901109868));
#34491=CARTESIAN_POINT('Ctrl Pts',(-22.8538386914514,26.6968583439427,-15.5481295101978));
#34492=CARTESIAN_POINT('Ctrl Pts',(-22.8522014918766,26.6964955484355,-15.5482336748758));
#34493=CARTESIAN_POINT('Ctrl Pts',(-22.8486957753428,26.6957158274978,-15.5484565999094));
#34494=CARTESIAN_POINT('Ctrl Pts',(-22.8468273518182,26.6952985160948,-15.5485753372829));
#34495=CARTESIAN_POINT('Ctrl Pts',(-22.8414068340739,26.6940827742929,-15.5489195971299));
#34496=CARTESIAN_POINT('Ctrl Pts',(-22.837855704882,26.6932799860401,-15.5491448677272));
#34497=CARTESIAN_POINT('Ctrl Pts',(-22.8218855626145,26.6896412293243,-15.5501568005669));
#34498=CARTESIAN_POINT('Ctrl Pts',(-22.8094818467412,26.6867376092168,-15.5509396078038));
#34499=CARTESIAN_POINT('Ctrl Pts',(-22.7892319830312,26.6818704351163,-15.5522129332371));
#34500=CARTESIAN_POINT('Ctrl Pts',(-22.781375584718,26.67995079383,-15.5527057991604));
#34501=CARTESIAN_POINT('Ctrl Pts',(-22.7649385393865,26.6758689182068,-15.5537347156383));
#34502=CARTESIAN_POINT('Ctrl Pts',(-22.7563593898575,26.6737008737209,-15.5542704604599));
#34503=CARTESIAN_POINT('Ctrl Pts',(-22.7452714847707,26.6708502043111,-15.5549613314683));
#34504=CARTESIAN_POINT('Ctrl Pts',(-22.7427545702257,26.6701998649943,-15.5551180539424));
#34505=CARTESIAN_POINT('Ctrl Pts',(-22.5945172986406,26.6317058078638,-15.5643425403541));
#34506=CARTESIAN_POINT('Ctrl Pts',(-22.4516080363896,26.5836953813842,-15.5729035730602));
#34507=CARTESIAN_POINT('Ctrl Pts',(-22.2318984448752,26.492308443191,-15.5862678891349));
#34508=CARTESIAN_POINT('Ctrl Pts',(-22.1526577784157,26.4555010185249,-15.5911313958584));
#34509=CARTESIAN_POINT('Ctrl Pts',(-22.0750358970872,26.4155367136697,-15.5960174792939));
#34510=CARTESIAN_POINT('Ctrl Pts',(-22.0750360164986,26.4155367751497,-15.845717117064));
#34511=CARTESIAN_POINT('Ctrl Pts',(-22.0813799877625,26.4188030239352,-15.845291974261));
#34512=CARTESIAN_POINT('Ctrl Pts',(-22.087734945045,26.4220482748863,-15.8448661251044));
#34513=CARTESIAN_POINT('Ctrl Pts',(-22.1320715052549,26.4445040355075,-15.841895188303));
#34514=CARTESIAN_POINT('Ctrl Pts',(-22.1704180126622,26.4629807419879,-15.8393259637509));
#34515=CARTESIAN_POINT('Ctrl Pts',(-22.2160638236638,26.48387084459,-15.836264188936));
#34516=CARTESIAN_POINT('Ctrl Pts',(-22.2230210375805,26.4870249903368,-15.8357974293847));
#34517=CARTESIAN_POINT('Ctrl Pts',(-22.2336947479676,26.4918183840204,-15.8350811657446));
#34518=CARTESIAN_POINT('Ctrl Pts',(-22.237403272247,26.4934754052109,-15.8348322734637));
#34519=CARTESIAN_POINT('Ctrl Pts',(-22.2441700864917,26.4964835795927,-15.834378069296));
#34520=CARTESIAN_POINT('Ctrl Pts',(-22.2472273696368,26.4978369949756,-15.8341728354432));
#34521=CARTESIAN_POINT('Ctrl Pts',(-22.2533768005446,26.5005478227503,-15.8337599807963));
#34522=CARTESIAN_POINT('Ctrl Pts',(-22.2564689865682,26.5019051373875,-15.8335523569673));
#34523=CARTESIAN_POINT('Ctrl Pts',(-22.2652706698497,26.5057521466903,-15.8329613003999));
#34524=CARTESIAN_POINT('Ctrl Pts',(-22.2709852364139,26.5082301424725,-15.8325774678101));
#34525=CARTESIAN_POINT('Ctrl Pts',(-22.2952451664967,26.5186664755345,-15.830947605066));
#34526=CARTESIAN_POINT('Ctrl Pts',(-22.3138575638419,26.5264669531227,-15.8296962032077));
#34527=CARTESIAN_POINT('Ctrl Pts',(-22.3369201692063,26.5358788487194,-15.8281441600935));
#34528=CARTESIAN_POINT('Ctrl Pts',(-22.3413025869535,26.5376560795097,-15.8278491734788));
#34529=CARTESIAN_POINT('Ctrl Pts',(-22.3564762710108,26.5437707071188,-15.8268275855064));
#34530=CARTESIAN_POINT('Ctrl Pts',(-22.3672869966791,26.5480592907115,-15.8260993437155));
#34531=CARTESIAN_POINT('Ctrl Pts',(-22.3817804029303,26.5537181770755,-15.8251224591094));
#34532=CARTESIAN_POINT('Ctrl Pts',(-22.3854428166297,26.5551404374495,-15.8248755568932));
#34533=CARTESIAN_POINT('Ctrl Pts',(-22.3960086662549,26.5592213563241,-15.8241631167938));
#34534=CARTESIAN_POINT('Ctrl Pts',(-22.4029186337065,26.5618629337149,-15.8236970134867));
#34535=CARTESIAN_POINT('Ctrl Pts',(-22.4241541826484,26.5698972748957,-15.8222640447014));
#34536=CARTESIAN_POINT('Ctrl Pts',(-22.4385089835142,26.5752117276235,-15.8212946179217));
#34537=CARTESIAN_POINT('Ctrl Pts',(-22.4596539947069,26.5828692200828,-15.819865444471));
#34538=CARTESIAN_POINT('Ctrl Pts',(-22.46641519784,26.5852921986497,-15.819408284113));
#34539=CARTESIAN_POINT('Ctrl Pts',(-22.4927574582739,26.5946330939844,-15.8176264506867));
#34540=CARTESIAN_POINT('Ctrl Pts',(-22.5123967784389,26.6013841647801,-15.8162965187948));
#34541=CARTESIAN_POINT('Ctrl Pts',(-22.5698463968849,26.6205137861791,-15.8124017477719));
#34542=CARTESIAN_POINT('Ctrl Pts',(-22.6078213665928,26.6323822581137,-15.8098216721482));
#34543=CARTESIAN_POINT('Ctrl Pts',(-22.8699560189756,26.7090108476705,-15.7919769809153));
#34544=CARTESIAN_POINT('Ctrl Pts',(-23.1003375778773,26.7499573158297,-15.7760483519954));
#34545=CARTESIAN_POINT('Ctrl Pts',(-23.4062189828573,26.770616713691,-15.7554066500887));
#34546=CARTESIAN_POINT('Ctrl Pts',(-23.4795079893906,26.7730599104725,-15.7505051089618));
#34547=CARTESIAN_POINT('Ctrl Pts',(-23.6243141498091,26.7729445556268,-15.7409778722624));
#34548=CARTESIAN_POINT('Ctrl Pts',(-23.6957933851422,26.770508527861,-15.7363509174702));
#34549=CARTESIAN_POINT('Ctrl Pts',(-23.7746016641019,26.7651928086171,-15.7313752416781));
#34550=CARTESIAN_POINT('Ctrl Pts',(-23.7820633175761,26.7646634076626,-15.7309053902673));
#34551=CARTESIAN_POINT('Ctrl Pts',(-23.7950761139163,26.7636946087277,-15.7300882522249));
#34552=CARTESIAN_POINT('Ctrl Pts',(-23.8006280502888,26.763266797093,-15.7297403373715));
#34553=CARTESIAN_POINT('Ctrl Pts',(-23.8086867627112,26.7626248077594,-15.7292364053266));
#34554=CARTESIAN_POINT('Ctrl Pts',(-23.811194401649,26.7624220839442,-15.729079746842));
#34555=CARTESIAN_POINT('Ctrl Pts',(-23.815593671767,26.7620612503294,-15.7288051808095));
#34556=CARTESIAN_POINT('Ctrl Pts',(-23.8174854030659,26.7619044054579,-15.7286872014067));
#34557=CARTESIAN_POINT('Ctrl Pts',(-23.8211469482804,26.7615975664508,-15.7284590153289));
#34558=CARTESIAN_POINT('Ctrl Pts',(-23.822916772335,26.7614477809913,-15.7283487969583));
#34559=CARTESIAN_POINT('Ctrl Pts',(-23.8271407295687,26.7610867777635,-15.7280859242587));
#34560=CARTESIAN_POINT('Ctrl Pts',(-23.8295947506074,26.7608742089836,-15.7279333466906));
#34561=CARTESIAN_POINT('Ctrl Pts',(-23.837011391256,26.7602232073652,-15.7274726535677));
#34562=CARTESIAN_POINT('Ctrl Pts',(-23.8419732699312,26.7597760779349,-15.7271650267466));
#34563=CARTESIAN_POINT('Ctrl Pts',(-23.8925684617701,26.7550984965022,-15.7240340190975));
#34564=CARTESIAN_POINT('Ctrl Pts',(-23.9381105100857,26.7499063525603,-15.7212638077876));
#34565=CARTESIAN_POINT('Ctrl Pts',(-24.2931767198342,26.7017327882941,-15.6999346360151));
#34566=CARTESIAN_POINT('Ctrl Pts',(-24.5951056189811,26.6149064423424,-15.6832574142852));
#34567=CARTESIAN_POINT('Ctrl Pts',(-24.9646544621277,26.4475363753833,-15.660098436646));
#34568=CARTESIAN_POINT('Ctrl Pts',(-25.0477579937007,26.4054691248088,-15.6547045569244));
#34569=CARTESIAN_POINT('Ctrl Pts',(-25.1806446106736,26.3308027271028,-15.6456772364674));
#34570=CARTESIAN_POINT('Ctrl Pts',(-25.2315544303152,26.3003181579484,-15.6421170677056));
#34571=CARTESIAN_POINT('Ctrl Pts',(-25.28971676101,26.2632719863008,-15.63791835879));
#34572=CARTESIAN_POINT('Ctrl Pts',(-25.2978186897424,26.258060295591,-15.6373304609273));
#34573=CARTESIAN_POINT('Ctrl Pts',(-25.3097801721264,26.250289843826,-15.636457966413));
#34574=CARTESIAN_POINT('Ctrl Pts',(-25.3136578258867,26.2477589306501,-15.6361744125689));
#34575=CARTESIAN_POINT('Ctrl Pts',(-25.3203846692324,26.2433476714415,-15.6356812705419));
#34576=CARTESIAN_POINT('Ctrl Pts',(-25.3232363578746,26.2414711344899,-15.6354718256897));
#34577=CARTESIAN_POINT('Ctrl Pts',(-25.3287184833864,26.2378511587163,-15.6350684346364));
#34578=CARTESIAN_POINT('Ctrl Pts',(-25.331349352985,26.2361083793467,-15.6348745134316));
#34579=CARTESIAN_POINT('Ctrl Pts',(-25.3375480649989,26.2319890244876,-15.6344168160085));
#34580=CARTESIAN_POINT('Ctrl Pts',(-25.3411137275117,26.2296091927585,-15.6341529169986));
#34581=CARTESIAN_POINT('Ctrl Pts',(-25.3534603374699,26.2213330328376,-15.6332369708439));
#34582=CARTESIAN_POINT('Ctrl Pts',(-25.3622169262856,26.2154006444354,-15.6325835590232));
#34583=CARTESIAN_POINT('Ctrl Pts',(-25.4663079619787,26.1441312372011,-15.6247705420027));
#34584=CARTESIAN_POINT('Ctrl Pts',(-25.558079226563,26.0737623146314,-15.6174174533563));
#34585=CARTESIAN_POINT('Ctrl Pts',(-25.8049739071177,25.8624399870858,-15.5962460504461));
#34586=CARTESIAN_POINT('Ctrl Pts',(-25.950413022526,25.7110833228611,-15.5820450288187));
#34587=CARTESIAN_POINT('Ctrl Pts',(-26.1889229446774,25.4088487210681,-15.5560128576535));
#34588=CARTESIAN_POINT('Ctrl Pts',(-26.2862836464221,25.2623013555872,-15.5442260783802));
#34589=CARTESIAN_POINT('Ctrl Pts',(-26.3770930086197,25.0979081113098,-15.5323862394424));
#34590=CARTESIAN_POINT('Ctrl Pts',(-26.3829017135751,25.0872507420613,-15.5316246324498));
#34591=CARTESIAN_POINT('Ctrl Pts',(-26.3902702045418,25.0735479334843,-15.5306532454589));
#34592=CARTESIAN_POINT('Ctrl Pts',(-26.3918854403425,25.0705326624424,-15.5304399793035));
#34593=CARTESIAN_POINT('Ctrl Pts',(-26.3944740264626,25.0656818331679,-15.5300976729679));
#34594=CARTESIAN_POINT('Ctrl Pts',(-26.3954504022205,25.0638479058544,-15.5299684393665));
#34595=CARTESIAN_POINT('Ctrl Pts',(-26.3973063649514,25.0603537081635,-15.5297225545905));
#34596=CARTESIAN_POINT('Ctrl Pts',(-26.3981862669506,25.0586936250894,-15.5296058838352));
#34597=CARTESIAN_POINT('Ctrl Pts',(-26.4001860697034,25.0549126739249,-15.5293404944994));
#34598=CARTESIAN_POINT('Ctrl Pts',(-26.4013050535352,25.0527913273603,-15.5291918350929));
#34599=CARTESIAN_POINT('Ctrl Pts',(-26.4047730343861,25.0461989778468,-15.5287305973293));
#34600=CARTESIAN_POINT('Ctrl Pts',(-26.4071139048033,25.0417236731195,-15.5284185357031));
#34601=CARTESIAN_POINT('Ctrl Pts',(-26.4248095737164,25.0076983605815,-15.5260538278495));
#34602=CARTESIAN_POINT('Ctrl Pts',(-26.4397167653928,24.9779160726506,-15.5240289861796));
#34603=CARTESIAN_POINT('Ctrl Pts',(-26.55590492653,24.7365117790282,-15.5079326470844));
#34604=CARTESIAN_POINT('Ctrl Pts',(-26.634277302723,24.5146075395105,-15.4950370647945));
#34605=CARTESIAN_POINT('Ctrl Pts',(-26.7197849948165,24.1500243582729,-15.4740794987766));
#34606=CARTESIAN_POINT('Ctrl Pts',(-26.7428152101527,24.011990136972,-15.4662014206117));
#34607=CARTESIAN_POINT('Ctrl Pts',(-26.7639174145687,23.8022740406461,-15.4539523746853));
#34608=CARTESIAN_POINT('Ctrl Pts',(-26.7686884655051,23.7314316681439,-15.4497687637593));
#34609=CARTESIAN_POINT('Ctrl Pts',(-26.7723734941796,23.6237673373602,-15.4433096994203));
#34610=CARTESIAN_POINT('Ctrl Pts',(-26.7730022290152,23.5870239997028,-15.4410876969372));
#34611=CARTESIAN_POINT('Ctrl Pts',(-26.7730025855875,23.5437208426695,-15.438445755659));
#34612=CARTESIAN_POINT('Ctrl Pts',(-26.7729826208195,23.5371626701843,-15.4380450124112));
#34613=CARTESIAN_POINT('Ctrl Pts',(-26.7729169399545,23.5263895499875,-15.4373856651596));
#34614=CARTESIAN_POINT('Ctrl Pts',(-26.772882972128,23.5221745281013,-15.4371274302223));
#34615=CARTESIAN_POINT('Ctrl Pts',(-26.7728071189599,23.5146049604687,-15.4366632010558));
#34616=CARTESIAN_POINT('Ctrl Pts',(-26.7727682647272,23.511250384815,-15.4364573022921));
#34617=CARTESIAN_POINT('Ctrl Pts',(-26.7726745900509,23.5041236640146,-15.4360195152071));
#34618=CARTESIAN_POINT('Ctrl Pts',(-26.7726183839737,23.5003515448623,-15.435787583679));
#34619=CARTESIAN_POINT('Ctrl Pts',(-26.772450303937,23.4902607179419,-15.4351665644317));
#34620=CARTESIAN_POINT('Ctrl Pts',(-26.7723264673371,23.483942249658,-15.4347771016143));
#34621=CARTESIAN_POINT('Ctrl Pts',(-26.7716514949522,23.4539991762576,-15.4329285412039));
#34622=CARTESIAN_POINT('Ctrl Pts',(-26.7708591222728,23.4303812269149,-15.4314618879537));
#34623=CARTESIAN_POINT('Ctrl Pts',(-26.7626441680427,23.2460427896882,-15.4199451220563));
#34624=CARTESIAN_POINT('Ctrl Pts',(-26.7434563323293,23.0860985169247,-15.4095220443941));
#34625=CARTESIAN_POINT('Ctrl Pts',(-26.65512144139,22.6370000216139,-15.3790871422077));
#34626=CARTESIAN_POINT('Ctrl Pts',(-26.5578662747802,22.3550567911624,-15.3584496253352));
#34627=CARTESIAN_POINT('Ctrl Pts',(-26.407116894781,22.0583623979864,-15.3370700950834));
#34628=CARTESIAN_POINT('Ctrl Pts',(-26.3902949867508,22.0265828551034,-15.3347870657845));
#34629=CARTESIAN_POINT('Ctrl Pts',(-26.3706993405364,21.9910158605267,-15.3322455219549));
#34630=CARTESIAN_POINT('Ctrl Pts',(-26.3684459273239,21.9869466807182,-15.3319549500272));
#34631=CARTESIAN_POINT('Ctrl Pts',(-26.3650264581359,21.9808032756401,-15.3315165860771));
#34632=CARTESIAN_POINT('Ctrl Pts',(-26.3638669140515,21.9787254616802,-15.3313683794264));
#34633=CARTESIAN_POINT('Ctrl Pts',(-26.3618484396901,21.9751179055519,-15.3311111593395));
#34634=CARTESIAN_POINT('Ctrl Pts',(-26.3609905616411,21.9735875808008,-15.3310020780096));
#34635=CARTESIAN_POINT('Ctrl Pts',(-26.3591941036806,21.9703890973018,-15.3307741574737));
#34636=CARTESIAN_POINT('Ctrl Pts',(-26.3582552878642,21.968721075312,-15.330655334256));
#34637=CARTESIAN_POINT('Ctrl Pts',(-26.3560096327567,21.9647394561019,-15.3303717887548));
#34638=CARTESIAN_POINT('Ctrl Pts',(-26.354701413187,21.9624266299491,-15.3302071559685));
#34639=CARTESIAN_POINT('Ctrl Pts',(-26.3502730028289,21.9546201053908,-15.3296517018959));
#34640=CARTESIAN_POINT('Ctrl Pts',(-26.3471394925309,21.9491339200525,-15.329261737773));
#34641=CARTESIAN_POINT('Ctrl Pts',(-26.3396632433027,21.9361333389742,-15.3283384876984));
#34642=CARTESIAN_POINT('Ctrl Pts',(-26.3353062175247,21.9286271565333,-15.3278061015328));
#34643=CARTESIAN_POINT('Ctrl Pts',(-26.2841109587621,21.8412441154336,-15.3216151174824));
#34644=CARTESIAN_POINT('Ctrl Pts',(-26.2338764552796,21.7633955489523,-15.3161655547298));
#34645=CARTESIAN_POINT('Ctrl Pts',(-25.9932168947353,21.4235410879099,-15.2921725922398));
#34646=CARTESIAN_POINT('Ctrl Pts',(-25.7673233880428,21.1889816048928,-15.2748489382622));
#34647=CARTESIAN_POINT('Ctrl Pts',(-25.4938751088604,20.9794795163518,-15.2546722553982));
#34648=CARTESIAN_POINT('Ctrl Pts',(-25.477389636887,20.9670984189246,-15.2534594308608));
#34649=CARTESIAN_POINT('Ctrl Pts',(-25.4571364479147,20.9521894381931,-15.2519731038887));
#34650=CARTESIAN_POINT('Ctrl Pts',(-25.4534804887665,20.9495100510011,-15.25170494813));
#34651=CARTESIAN_POINT('Ctrl Pts',(-25.4465816105758,20.9444763236278,-15.2511991954427));
#34652=CARTESIAN_POINT('Ctrl Pts',(-25.4433399265044,20.9421203001262,-15.2509616585829));
#34653=CARTESIAN_POINT('Ctrl Pts',(-25.4358985204637,20.9367331433962,-15.2504166255318));
#34654=CARTESIAN_POINT('Ctrl Pts',(-25.4316958761873,20.9337060809331,-15.250108985859));
#34655=CARTESIAN_POINT('Ctrl Pts',(-25.4218731858701,20.9266669373007,-15.2493903427809));
#34656=CARTESIAN_POINT('Ctrl Pts',(-25.4162475203116,20.922662771927,-15.2489790586655));
#34657=CARTESIAN_POINT('Ctrl Pts',(-25.4086482448746,20.9172905680487,-15.2484238648719));
#34658=CARTESIAN_POINT('Ctrl Pts',(-25.4066858843158,20.9159065908581,-15.2482805310533));
#34659=CARTESIAN_POINT('Ctrl Pts',(-25.4026925172639,20.9130969010916,-15.2479889167728));
#34660=CARTESIAN_POINT('Ctrl Pts',(-25.4006614075377,20.9116713386464,-15.2478406310191));
#34661=CARTESIAN_POINT('Ctrl Pts',(-25.3932662750824,20.906493700969,-15.2473008584088));
#34662=CARTESIAN_POINT('Ctrl Pts',(-25.3878924956088,20.9027556430378,-15.2469088651587));
#34663=CARTESIAN_POINT('Ctrl Pts',(-25.3769126324925,20.8951674690088,-15.2461083944734));
#34664=CARTESIAN_POINT('Ctrl Pts',(-25.3713056786125,20.8913186759953,-15.2456998715153));
#34665=CARTESIAN_POINT('Ctrl Pts',(-25.3426373520131,20.8717730307061,-15.2436122625739));
#34666=CARTESIAN_POINT('Ctrl Pts',(-25.3193855985676,20.8563587146079,-15.2419229100669));
#34667=CARTESIAN_POINT('Ctrl Pts',(-25.2897780160384,20.8372795608588,-15.239775449887));
#34668=CARTESIAN_POINT('Ctrl Pts',(-25.2836053382168,20.8333316094204,-15.2393279410292));
#34669=CARTESIAN_POINT('Ctrl Pts',(-25.2737030048101,20.8270457078997,-15.238610335863));
#34670=CARTESIAN_POINT('Ctrl Pts',(-25.2699819047533,20.8246942729924,-15.2383407410542));
#34671=CARTESIAN_POINT('Ctrl Pts',(-25.2633876635326,20.8205461251951,-15.2378630996283));
#34672=CARTESIAN_POINT('Ctrl Pts',(-25.2605164782831,20.8187463028015,-15.2376551686393));
#34673=CARTESIAN_POINT('Ctrl Pts',(-25.2545565558345,20.8150233649697,-15.2372236275006));
#34674=CARTESIAN_POINT('Ctrl Pts',(-25.2514673911508,20.8131009460139,-15.2369999919904));
#34675=CARTESIAN_POINT('Ctrl Pts',(-25.243513407324,20.8081697669455,-15.2364242796221));
#34676=CARTESIAN_POINT('Ctrl Pts',(-25.2386438366384,20.8051687292605,-15.2360719185691));
#34677=CARTESIAN_POINT('Ctrl Pts',(-25.2187764479559,20.7929976417427,-15.2346347042834));
#34678=CARTESIAN_POINT('Ctrl Pts',(-25.2037119289596,20.7839375479681,-15.2335458216456));
#34679=CARTESIAN_POINT('Ctrl Pts',(-25.1035346607323,20.724799623857,-15.2263098194471));
#34680=CARTESIAN_POINT('Ctrl Pts',(-25.0162410419218,20.6785381014474,-15.2200254040262));
#34681=CARTESIAN_POINT('Ctrl Pts',(-24.7937174754043,20.573403193626,-15.204039513471));
#34682=CARTESIAN_POINT('Ctrl Pts',(-24.6563179839261,20.5196670850238,-15.1941919238845));
#34683=CARTESIAN_POINT('Ctrl Pts',(-24.3265512654169,20.4161181249453,-15.1708489076429));
#34684=CARTESIAN_POINT('Ctrl Pts',(-24.132276834729,20.374296874546,-15.1573064641323));
#34685=CARTESIAN_POINT('Ctrl Pts',(-23.9275096798446,20.3496498564076,-15.1438961827688));
#34686=CARTESIAN_POINT('Ctrl Pts',(-23.9196333702916,20.3487312933848,-15.1433817176381));
#34687=CARTESIAN_POINT('Ctrl Pts',(-23.9078961836278,20.3474063520275,-15.142617164907));
#34688=CARTESIAN_POINT('Ctrl Pts',(-23.904037888688,20.3469778706898,-15.1423661753869));
#34689=CARTESIAN_POINT('Ctrl Pts',(-23.8971419425714,20.3462246554553,-15.1419181942622));
#34690=CARTESIAN_POINT('Ctrl Pts',(-23.8941045927834,20.3458972681001,-15.1417210915612));
#34691=CARTESIAN_POINT('Ctrl Pts',(-23.8849707468724,20.3449258929987,-15.1411290169273));
#34692=CARTESIAN_POINT('Ctrl Pts',(-23.8788728371517,20.3442949773366,-15.1407346055066));
#34693=CARTESIAN_POINT('Ctrl Pts',(-23.8377371149947,20.3401574993735,-15.138079968241));
#34694=CARTESIAN_POINT('Ctrl Pts',(-23.8026438847066,20.3372078135023,-15.1358446622168));
#34695=CARTESIAN_POINT('Ctrl Pts',(-23.7628949828957,20.3345221132771,-15.1333513059536));
#34696=CARTESIAN_POINT('Ctrl Pts',(-23.7582816535313,20.3342203768352,-15.1330625085419));
#34697=CARTESIAN_POINT('Ctrl Pts',(-23.7513002071158,20.333778838044,-15.1326263684331));
#34698=CARTESIAN_POINT('Ctrl Pts',(-23.7489325834987,20.3336317230131,-15.1324786169728));
#34699=CARTESIAN_POINT('Ctrl Pts',(-23.7448155167525,20.3333804672967,-15.1322219672592));
#34700=CARTESIAN_POINT('Ctrl Pts',(-23.7430661513904,20.3332751394905,-15.1321130018458));
#34701=CARTESIAN_POINT('Ctrl Pts',(-23.7394043951533,20.3330576658455,-15.1318850987389));
#34702=CARTESIAN_POINT('Ctrl Pts',(-23.7374919912631,20.3329457982453,-15.1317661773513));
#34703=CARTESIAN_POINT('Ctrl Pts',(-23.7329181215214,20.332682338031,-15.131482001677));
#34704=CARTESIAN_POINT('Ctrl Pts',(-23.7302565572012,20.3325323419044,-15.1313168379325));
#34705=CARTESIAN_POINT('Ctrl Pts',(-23.7213643561069,20.3320422771646,-15.1307656898636));
#34706=CARTESIAN_POINT('Ctrl Pts',(-23.7151328681393,20.3317169990321,-15.1303805358634));
#34707=CARTESIAN_POINT('Ctrl Pts',(-23.7003007211742,20.3309859634074,-15.1294662820104));
#34708=CARTESIAN_POINT('Ctrl Pts',(-23.6916992523223,20.3305965677801,-15.1289380767818));
#34709=CARTESIAN_POINT('Ctrl Pts',(-23.5919088450246,20.3264796484286,-15.1228320820669));
#34710=CARTESIAN_POINT('Ctrl Pts',(-23.5005931377506,20.3265924635539,-15.1174574329503));
#34711=CARTESIAN_POINT('Ctrl Pts',(-23.1484524519573,20.3419981112915,-15.0971352997133));
#34712=CARTESIAN_POINT('Ctrl Pts',(-22.8898551646639,20.385093417396,-15.0829931804492));
#34713=CARTESIAN_POINT('Ctrl Pts',(-22.5818456323604,20.4758597367537,-15.0646383215396));
#34714=CARTESIAN_POINT('Ctrl Pts',(-22.5248944891357,20.4943822253599,-15.0611822486005));
#34715=CARTESIAN_POINT('Ctrl Pts',(-22.446950456237,20.5221565676844,-15.0563437844396));
#34716=CARTESIAN_POINT('Ctrl Pts',(-22.4254892626766,20.5300624399978,-15.0550000343342));
#34717=CARTESIAN_POINT('Ctrl Pts',(-22.3994647183322,20.5399652163467,-15.0533555906488));
#34718=CARTESIAN_POINT('Ctrl Pts',(-22.3948191645827,20.5417452529742,-15.0530614627599));
#34719=CARTESIAN_POINT('Ctrl Pts',(-22.386467372297,20.544967606481,-15.0525316147014));
#34720=CARTESIAN_POINT('Ctrl Pts',(-22.3827596405654,20.5464060429548,-15.0522960134086));
#34721=CARTESIAN_POINT('Ctrl Pts',(-22.3666176395726,20.5527028291119,-15.0512686343233));
#34722=CARTESIAN_POINT('Ctrl Pts',(-22.3542110877954,20.5576315008724,-15.0504746953763));
#34723=CARTESIAN_POINT('Ctrl Pts',(-22.339565186803,20.5635554071477,-15.0495321943651));
#34724=CARTESIAN_POINT('Ctrl Pts',(-22.3372957775286,20.5644763389212,-15.0493860022005));
#34725=CARTESIAN_POINT('Ctrl Pts',(-22.3328734094752,20.5662768206442,-15.0491008256321));
#34726=CARTESIAN_POINT('Ctrl Pts',(-22.3307203482195,20.567156116092,-15.0489618494371));
#34727=CARTESIAN_POINT('Ctrl Pts',(-22.3223960111388,20.5705662365963,-15.0484240000634));
#34728=CARTESIAN_POINT('Ctrl Pts',(-22.3162316767447,20.5731138750599,-15.0480245876063));
#34729=CARTESIAN_POINT('Ctrl Pts',(-22.3032396558225,20.5785305900096,-15.047180375264));
#34730=CARTESIAN_POINT('Ctrl Pts',(-22.2964138693841,20.58140409858,-15.0467354329798));
#34731=CARTESIAN_POINT('Ctrl Pts',(-22.262945031639,20.595629766057,-15.0445467372489));
#34732=CARTESIAN_POINT('Ctrl Pts',(-22.2364465879361,20.6073168978924,-15.0427919823008));
#34733=CARTESIAN_POINT('Ctrl Pts',(-22.204266186974,20.6220312950076,-15.0406328708845));
#34734=CARTESIAN_POINT('Ctrl Pts',(-22.1984305137233,20.624720771152,-15.040240194337));
#34735=CARTESIAN_POINT('Ctrl Pts',(-22.1888174506451,20.6291860304856,-15.0395914461875));
#34736=CARTESIAN_POINT('Ctrl Pts',(-22.1850353791303,20.6309517403266,-15.0393357235571));
#34737=CARTESIAN_POINT('Ctrl Pts',(-22.1782231421844,20.6341482561339,-15.0388742378581));
#34738=CARTESIAN_POINT('Ctrl Pts',(-22.175191752963,20.6355764525595,-15.0386685655761));
#34739=CARTESIAN_POINT('Ctrl Pts',(-22.1687281500936,20.6386340160737,-15.0382293509754));
#34740=CARTESIAN_POINT('Ctrl Pts',(-22.165296581795,20.6402647286093,-15.0379957621126));
#34741=CARTESIAN_POINT('Ctrl Pts',(-22.1561727198709,20.644620265264,-15.0373736070515));
#34742=CARTESIAN_POINT('Ctrl Pts',(-22.150485553824,20.6473557377639,-15.036984670349));
#34743=CARTESIAN_POINT('Ctrl Pts',(-22.1234742380787,20.6604457561386,-15.0351319927094));
#34744=CARTESIAN_POINT('Ctrl Pts',(-22.1022571708309,20.6710184519921,-15.0336606433234));
#34745=CARTESIAN_POINT('Ctrl Pts',(-21.9362074498903,20.7560624232953,-15.0220156417662));
#34746=CARTESIAN_POINT('Ctrl Pts',(-21.797114655308,20.8411691360699,-15.0114594648272));
#34747=CARTESIAN_POINT('Ctrl Pts',(-21.4887398583535,21.0635788785438,-14.9861623451807));
#34748=CARTESIAN_POINT('Ctrl Pts',(-21.3257478223474,21.2082552288599,-14.9712490047915));
#34749=CARTESIAN_POINT('Ctrl Pts',(-21.14955622988,21.3997617663604,-14.9539046234572));
#34750=CARTESIAN_POINT('Ctrl Pts',(-21.1211777137389,21.4318689331248,-14.9510689535246));
#34751=CARTESIAN_POINT('Ctrl Pts',(-21.0896486173265,21.469007619922,-14.9478780898256));
#34752=CARTESIAN_POINT('Ctrl Pts',(-21.0858625682158,21.4734920459962,-14.9474942465429));
#34753=CARTESIAN_POINT('Ctrl Pts',(-21.0734704505337,21.4882516280451,-14.9462357125665));
#34754=CARTESIAN_POINT('Ctrl Pts',(-21.0649161178238,21.4985702645475,-14.9453634726955));
#34755=CARTESIAN_POINT('Ctrl Pts',(-21.0548315954411,21.5108903147397,-14.9443313470368));
#34756=CARTESIAN_POINT('Ctrl Pts',(-21.0532392006373,21.5128403678239,-14.9441682538802));
#34757=CARTESIAN_POINT('Ctrl Pts',(-21.0499396005216,21.5168907501636,-14.9438300720318));
#34758=CARTESIAN_POINT('Ctrl Pts',(-21.0482327519047,21.5189913692589,-14.9436550020984));
#34759=CARTESIAN_POINT('Ctrl Pts',(-21.0181159438763,21.5561516890539,-14.9405636478855));
#34760=CARTESIAN_POINT('Ctrl Pts',(-20.9904409478681,21.5918044103815,-14.9376866544317));
#34761=CARTESIAN_POINT('Ctrl Pts',(-20.9602782471072,21.632394260582,-14.9345202668162));
#34762=CARTESIAN_POINT('Ctrl Pts',(-20.9570452863316,21.6367679285355,-14.9341804709735));
#34763=CARTESIAN_POINT('Ctrl Pts',(-20.9524693488718,21.6429913219565,-14.9336989647292));
#34764=CARTESIAN_POINT('Ctrl Pts',(-20.9511172671283,21.6448342931716,-14.9335566212587));
#34765=CARTESIAN_POINT('Ctrl Pts',(-20.948642323886,21.6482153302827,-14.9332959404141));
#34766=CARTESIAN_POINT('Ctrl Pts',(-20.9475188632435,21.6497529552411,-14.9331775609276));
#34767=CARTESIAN_POINT('Ctrl Pts',(-20.9452347033954,21.6528849958458,-14.9329367825747));
#34768=CARTESIAN_POINT('Ctrl Pts',(-20.9440741047289,21.6544794812693,-14.932814390796));
#34769=CARTESIAN_POINT('Ctrl Pts',(-20.9412195049727,21.6584088412133,-14.9325132296502));
#34770=CARTESIAN_POINT('Ctrl Pts',(-20.9395271695759,21.6607449324811,-14.932334577064));
#34771=CARTESIAN_POINT('Ctrl Pts',(-20.9332660503652,21.6694122203887,-14.9316731937273));
#34772=CARTESIAN_POINT('Ctrl Pts',(-20.9287170934505,21.67575780801,-14.9311918327046));
#34773=CARTESIAN_POINT('Ctrl Pts',(-20.8143787534156,21.8364848874251,-14.9190697481409));
#34774=CARTESIAN_POINT('Ctrl Pts',(-20.7183716003689,22.0002592467038,-14.9083413770415));
#34775=CARTESIAN_POINT('Ctrl Pts',(-20.5611010005301,22.3325426378547,-14.8877389942324));
#34776=CARTESIAN_POINT('Ctrl Pts',(-20.4983817541327,22.4995734847129,-14.8778813714213));
#34777=CARTESIAN_POINT('Ctrl Pts',(-20.4342405348895,22.7257332738947,-14.8644040002754));
#34778=CARTESIAN_POINT('Ctrl Pts',(-20.4201537071223,22.7809387849163,-14.8611062794753));
#34779=CARTESIAN_POINT('Ctrl Pts',(-20.4033270067,22.8550268340747,-14.8566526366753));
#34780=CARTESIAN_POINT('Ctrl Pts',(-20.3992804203139,22.8736036101323,-14.8555336380128));
#34781=CARTESIAN_POINT('Ctrl Pts',(-20.3944464214141,22.8967794268848,-14.8541342452425));
#34782=CARTESIAN_POINT('Ctrl Pts',(-20.3935042537894,22.9013460561374,-14.8538583428607));
#34783=CARTESIAN_POINT('Ctrl Pts',(-20.3917645199682,22.9098718997552,-14.853342923482));
#34784=CARTESIAN_POINT('Ctrl Pts',(-20.3909644784546,22.9138306037025,-14.8531034791949));
#34785=CARTESIAN_POINT('Ctrl Pts',(-20.3894113630448,22.9215907093599,-14.8526338518122));
#34786=CARTESIAN_POINT('Ctrl Pts',(-20.3886576999869,22.9253919870724,-14.8524036864686));
#34787=CARTESIAN_POINT('Ctrl Pts',(-20.3777153550909,22.9811089037282,-14.8490282684573));
#34788=CARTESIAN_POINT('Ctrl Pts',(-20.3688002150822,23.0332638826459,-14.8458456954992));
#34789=CARTESIAN_POINT('Ctrl Pts',(-20.3599143725103,23.0942522860705,-14.8420897697068));
#34790=CARTESIAN_POINT('Ctrl Pts',(-20.3586906968907,23.1028971402921,-14.8415565885755));
#34791=CARTESIAN_POINT('Ctrl Pts',(-20.3569184700033,23.1157948016147,-14.8407598924292));
#34792=CARTESIAN_POINT('Ctrl Pts',(-20.3563432455858,23.1200439536645,-14.840497222864));
#34793=CARTESIAN_POINT('Ctrl Pts',(-20.3553320506602,23.127627414055,-14.8400280806362));
#34794=CARTESIAN_POINT('Ctrl Pts',(-20.3548928145463,23.1309612867553,-14.8398217117056));
#34795=CARTESIAN_POINT('Ctrl Pts',(-20.3539774215546,23.1379942475896,-14.8393861055743));
#34796=CARTESIAN_POINT('Ctrl Pts',(-20.3535024667847,23.1416934847683,-14.8391568306451));
#34797=CARTESIAN_POINT('Ctrl Pts',(-20.3522794967798,23.1513514209479,-14.8385578400213));
#34798=CARTESIAN_POINT('Ctrl Pts',(-20.3515417164861,23.1573113807776,-14.8381878010729));
#34799=CARTESIAN_POINT('Ctrl Pts',(-20.3483534574062,23.1836709835844,-14.8365494085477));
#34800=CARTESIAN_POINT('Ctrl Pts',(-20.3460814798355,23.2040913665023,-14.8352754265874));
#34801=CARTESIAN_POINT('Ctrl Pts',(-20.3352535773325,23.3106763104763,-14.8285999921787));
#34802=CARTESIAN_POINT('Ctrl Pts',(-20.3299782301424,23.3971311765341,-14.8230959654542));
#34803=CARTESIAN_POINT('Ctrl Pts',(-20.3255123560234,23.6133000402341,-14.8090989465709));
#34804=CARTESIAN_POINT('Ctrl Pts',(-20.3306580888177,23.7429435771971,-14.8004897463206));
#34805=CARTESIAN_POINT('Ctrl Pts',(-20.3584274325684,24.0197776728857,-14.781769525876));
#34806=CARTESIAN_POINT('Ctrl Pts',(-20.3834690051902,24.1664368443192,-14.7716432392594));
#34807=CARTESIAN_POINT('Ctrl Pts',(-20.4424297874457,24.4092060427564,-14.7548999727367));
#34808=CARTESIAN_POINT('Ctrl Pts',(-20.4709419921012,24.5063978188601,-14.7482055187393));
#34809=CARTESIAN_POINT('Ctrl Pts',(-20.5054214269573,24.6062546521523,-14.7414417449694));
#34810=CARTESIAN_POINT('Ctrl Pts',(-20.506866485453,24.6104120993058,-14.7411603546057));
#34811=CARTESIAN_POINT('Ctrl Pts',(-20.510025620634,24.619441272345,-14.7405497121778));
#34812=CARTESIAN_POINT('Ctrl Pts',(-20.5117429039002,24.6243118766444,-14.7402206197781));
#34813=CARTESIAN_POINT('Ctrl Pts',(-20.516186167569,24.6368180347194,-14.7393764409498));
#34814=CARTESIAN_POINT('Ctrl Pts',(-20.5189292861293,24.6444475226649,-14.7388622347415));
#34815=CARTESIAN_POINT('Ctrl Pts',(-20.5231807694212,24.6561335547935,-14.7380759333394));
#34816=CARTESIAN_POINT('Ctrl Pts',(-20.5246685395587,24.6601974844839,-14.7378027321635));
#34817=CARTESIAN_POINT('Ctrl Pts',(-20.5301667886824,24.6751230691417,-14.7368002716573));
#34818=CARTESIAN_POINT('Ctrl Pts',(-20.5342276703386,24.6859662573128,-14.7360738030184));
#34819=CARTESIAN_POINT('Ctrl Pts',(-20.5395951458232,24.7000664194689,-14.7351316979496));
#34820=CARTESIAN_POINT('Ctrl Pts',(-20.5408486777127,24.7033432980869,-14.7349129343708));
#34821=CARTESIAN_POINT('Ctrl Pts',(-20.5427849683427,24.7083803234547,-14.7345769507794));
#34822=CARTESIAN_POINT('Ctrl Pts',(-20.5434639216875,24.7101419149702,-14.7344595017787));
#34823=CARTESIAN_POINT('Ctrl Pts',(-20.5448166476947,24.71364248681,-14.7342262202607));
#34824=CARTESIAN_POINT('Ctrl Pts',(-20.5454903780316,24.715381468956,-14.7341103865274));
#34825=CARTESIAN_POINT('Ctrl Pts',(-20.5469958550077,24.7192573025565,-14.7338523361302));
#34826=CARTESIAN_POINT('Ctrl Pts',(-20.5478283709625,24.7213938466064,-14.7337101670389));
#34827=CARTESIAN_POINT('Ctrl Pts',(-20.5502347503358,24.7275500764412,-14.7333007489261));
#34828=CARTESIAN_POINT('Ctrl Pts',(-20.5518144185634,24.7315675106792,-14.7330338503929));
#34829=CARTESIAN_POINT('Ctrl Pts',(-20.5616528587383,24.7564418929862,-14.7313829814962));
#34830=CARTESIAN_POINT('Ctrl Pts',(-20.5701214042584,24.7772159830804,-14.730011492275));
#34831=CARTESIAN_POINT('Ctrl Pts',(-20.5969375456606,24.8410823228437,-14.7258125475855));
#34832=CARTESIAN_POINT('Ctrl Pts',(-20.6160088080624,24.883866128188,-14.7230244266254));
#34833=CARTESIAN_POINT('Ctrl Pts',(-20.6627493829402,24.9828607495343,-14.7165972218532));
#34834=CARTESIAN_POINT('Ctrl Pts',(-20.6911387562169,25.0387114531932,-14.7129896101063));
#34835=CARTESIAN_POINT('Ctrl Pts',(-20.7962740363095,25.2314224174036,-14.7004883415939));
#34836=CARTESIAN_POINT('Ctrl Pts',(-20.8813669134498,25.3634769151451,-14.6918159071477));
#34837=CARTESIAN_POINT('Ctrl Pts',(-21.0048959758671,25.5275301072561,-14.6802936892157));
#34838=CARTESIAN_POINT('Ctrl Pts',(-21.0349191858624,25.5655849142249,-14.6775643528621));
#34839=CARTESIAN_POINT('Ctrl Pts',(-21.1756124023363,25.7358718842449,-14.6650392326436));
#34840=CARTESIAN_POINT('Ctrl Pts',(-21.2959098931277,25.8597489709747,-14.6550251769472));
#34841=CARTESIAN_POINT('Ctrl Pts',(-21.4341513639941,25.9809653977659,-14.6438442572034));
#34842=CARTESIAN_POINT('Ctrl Pts',(-21.442817924519,25.9884831525354,-14.6431446666558));
#34843=CARTESIAN_POINT('Ctrl Pts',(-21.4548930284213,25.9988451517449,-14.6421717268801));
#34844=CARTESIAN_POINT('Ctrl Pts',(-21.4582676561704,26.0017289332085,-14.6419000128294));
#34845=CARTESIAN_POINT('Ctrl Pts',(-21.4640817501095,26.0066766081129,-14.6414322077035));
#34846=CARTESIAN_POINT('Ctrl Pts',(-21.4665183543875,26.0087438681363,-14.6412362555106));
#34847=CARTESIAN_POINT('Ctrl Pts',(-21.4715457622532,26.0129963707386,-14.6408321505107));
#34848=CARTESIAN_POINT('Ctrl Pts',(-21.4741369453984,26.0151811558684,-14.6406239793256));
#34849=CARTESIAN_POINT('Ctrl Pts',(-21.4801627530997,26.0202456410813,-14.6401401265828));
#34850=CARTESIAN_POINT('Ctrl Pts',(-21.4835999420538,26.0231222664901,-14.6398643196902));
#34851=CARTESIAN_POINT('Ctrl Pts',(-21.4944357788327,26.032152539488,-14.63899541322));
#34852=CARTESIAN_POINT('Ctrl Pts',(-21.5018559431566,26.0382801808326,-14.6384012552909));
#34853=CARTESIAN_POINT('Ctrl Pts',(-21.5730700978168,26.0965549861105,-14.6327067719172));
#34854=CARTESIAN_POINT('Ctrl Pts',(-21.6388091902006,26.1462665728181,-14.6275090496299));
#34855=CARTESIAN_POINT('Ctrl Pts',(-21.7647508544295,26.2341242270233,-14.6176442001909));
#34856=CARTESIAN_POINT('Ctrl Pts',(-21.8244550853129,26.2728993196253,-14.6130040539844));
#34857=CARTESIAN_POINT('Ctrl Pts',(-21.9474214609267,26.3470897849638,-14.6035273748634));
#34858=CARTESIAN_POINT('Ctrl Pts',(-22.0106735371924,26.3823991979172,-14.5986930264539));
#34859=CARTESIAN_POINT('Ctrl Pts',(-22.0750361948364,26.4155368669684,-14.5938261690085));
#34860=CARTESIAN_POINT('Origin',(-23.5502525316942,23.5502525316942,-77.3107734492734));
#34861=CARTESIAN_POINT('',(-22.0750356748951,26.4155365992721,-13.0947094732148));
#34862=CARTESIAN_POINT('',(-22.0750360153462,26.4155367745563,-13.3428506325468));
#34863=CARTESIAN_POINT('',(-22.0750360153461,26.4155367745563,-77.3107734492734));
#34864=CARTESIAN_POINT('Ctrl Pts',(-22.0750356748951,26.4155365992721,-13.0947094732148));
#34865=CARTESIAN_POINT('Ctrl Pts',(-22.0083520106634,26.3812039246655,-13.0997046728913));
#34866=CARTESIAN_POINT('Ctrl Pts',(-21.9428598907341,26.3445397821812,-13.1047516267623));
#34867=CARTESIAN_POINT('Ctrl Pts',(-21.7610611649787,26.2342491824425,-13.119116417468));
#34868=CARTESIAN_POINT('Ctrl Pts',(-21.6481287722094,26.1554339924971,-13.1284745675161));
#34869=CARTESIAN_POINT('Ctrl Pts',(-21.4983837045451,26.0359848078024,-13.141245825012));
#34870=CARTESIAN_POINT('Ctrl Pts',(-21.4570403577237,26.0012715034878,-13.1448129245727));
#34871=CARTESIAN_POINT('Ctrl Pts',(-21.3857261608882,25.9382723684787,-13.1510131155592));
#34872=CARTESIAN_POINT('Ctrl Pts',(-21.3553894285417,25.9104197860558,-13.1536665338162));
#34873=CARTESIAN_POINT('Ctrl Pts',(-21.3106573097603,25.867741896068,-13.1575923808026));
#34874=CARTESIAN_POINT('Ctrl Pts',(-21.2958580943671,25.8533481629355,-13.1588934761794));
#34875=CARTESIAN_POINT('Ctrl Pts',(-21.2783066200613,25.8359462803271,-13.1604381368472));
#34876=CARTESIAN_POINT('Ctrl Pts',(-21.275420902497,25.8330742937169,-13.1606921538052));
#34877=CARTESIAN_POINT('Ctrl Pts',(-21.2709689260576,25.8286266763774,-13.1610841111566));
#34878=CARTESIAN_POINT('Ctrl Pts',(-21.2693988542205,25.827054894683,-13.1612223555892));
#34879=CARTESIAN_POINT('Ctrl Pts',(-21.2666451025541,25.8242924369837,-13.1614648442129));
#34880=CARTESIAN_POINT('Ctrl Pts',(-21.2654607326394,25.8231024643297,-13.161569143783));
#34881=CARTESIAN_POINT('Ctrl Pts',(-21.2627531404233,25.8203778085975,-13.1618075991007));
#34882=CARTESIAN_POINT('Ctrl Pts',(-21.2612305352458,25.8188425205952,-13.1619417052926));
#34883=CARTESIAN_POINT('Ctrl Pts',(-21.257105350445,25.8146745930104,-13.1623050739833));
#34884=CARTESIAN_POINT('Ctrl Pts',(-21.2545057497669,25.812038989396,-13.1625340994643));
#34885=CARTESIAN_POINT('Ctrl Pts',(-21.2422859047403,25.7996071338631,-13.1636108870893));
#34886=CARTESIAN_POINT('Ctrl Pts',(-21.2327235988285,25.7897537571136,-13.1644541304079));
#34887=CARTESIAN_POINT('Ctrl Pts',(-21.0548731149077,25.6041305370049,-13.18015662214));
#34888=CARTESIAN_POINT('Ctrl Pts',(-20.9069334782329,25.4098867635605,-13.1935737466354));
#34889=CARTESIAN_POINT('Ctrl Pts',(-20.7064538541379,25.073681034789,-13.2154580544452));
#34890=CARTESIAN_POINT('Ctrl Pts',(-20.6394999607987,24.9414895186487,-13.2237700450278));
#34891=CARTESIAN_POINT('Ctrl Pts',(-20.5529211488902,24.7366964856991,-13.2366664155525));
#34892=CARTESIAN_POINT('Ctrl Pts',(-20.5263517520093,24.6672429172322,-13.2410412451782));
#34893=CARTESIAN_POINT('Ctrl Pts',(-20.4941073951359,24.5733442626343,-13.2469897713353));
#34894=CARTESIAN_POINT('Ctrl Pts',(-20.4862803193698,24.5496593631594,-13.248492969221));
#34895=CARTESIAN_POINT('Ctrl Pts',(-20.4753900969882,24.5153744012985,-13.2506738442773));
#34896=CARTESIAN_POINT('Ctrl Pts',(-20.4721050758065,24.5048453509938,-13.251344263924));
#34897=CARTESIAN_POINT('Ctrl Pts',(-20.4663631611793,24.4861036916264,-13.2525388771142));
#34898=CARTESIAN_POINT('Ctrl Pts',(-20.4638848518499,24.477897714777,-13.2530623654408));
#34899=CARTESIAN_POINT('Ctrl Pts',(-20.4602304707623,24.4656208617771,-13.2538462252109));
#34900=CARTESIAN_POINT('Ctrl Pts',(-20.4590296269875,24.4615573489257,-13.2541057851366));
#34901=CARTESIAN_POINT('Ctrl Pts',(-20.456925077583,24.4543837795141,-13.2545642012833));
#34902=CARTESIAN_POINT('Ctrl Pts',(-20.4560180378703,24.4512747005381,-13.2547629481559));
#34903=CARTESIAN_POINT('Ctrl Pts',(-20.4542182256958,24.4450706776469,-13.2551596717967));
#34904=CARTESIAN_POINT('Ctrl Pts',(-20.4533254035659,24.4419757517469,-13.255357646691));
#34905=CARTESIAN_POINT('Ctrl Pts',(-20.451186687573,24.4345200393279,-13.2558347322538));
#34906=CARTESIAN_POINT('Ctrl Pts',(-20.4499453584229,24.4301579597323,-13.2561139916314));
#34907=CARTESIAN_POINT('Ctrl Pts',(-20.4461624441928,24.4167572619743,-13.2569723182806));
#34908=CARTESIAN_POINT('Ctrl Pts',(-20.4436511648223,24.4077102060295,-13.2575523721091));
#34909=CARTESIAN_POINT('Ctrl Pts',(-20.4345369445851,24.374309944865,-13.2596960631648));
#34910=CARTESIAN_POINT('Ctrl Pts',(-20.4281806817739,24.3498909158756,-13.2612676870682));
#34911=CARTESIAN_POINT('Ctrl Pts',(-20.4206598747981,24.3195403917495,-13.2632268943196));
#34912=CARTESIAN_POINT('Ctrl Pts',(-20.4192242730923,24.3136764327889,-13.2636056964035));
#34913=CARTESIAN_POINT('Ctrl Pts',(-20.4161913656122,24.3011355468805,-13.264416397071));
#34914=CARTESIAN_POINT('Ctrl Pts',(-20.4145989036689,24.2944574894287,-13.2648484482815));
#34915=CARTESIAN_POINT('Ctrl Pts',(-20.4127144885043,24.2864416815978,-13.2653674743066));
#34916=CARTESIAN_POINT('Ctrl Pts',(-20.4124020244989,24.2851087294528,-13.2654537974869));
#34917=CARTESIAN_POINT('Ctrl Pts',(-20.3410933139109,23.9800354329428,-13.2852138569727));
#34918=CARTESIAN_POINT('Ctrl Pts',(-20.3145843724405,23.6676468020343,-13.3064256333339));
#34919=CARTESIAN_POINT('Ctrl Pts',(-20.3383290956884,23.2735658166588,-13.3330358993233));
#34920=CARTESIAN_POINT('Ctrl Pts',(-20.3465210644565,23.1909283189385,-13.3385918738686));
#34921=CARTESIAN_POINT('Ctrl Pts',(-20.3672685944779,23.0409284463298,-13.3485389577744));
#34922=CARTESIAN_POINT('Ctrl Pts',(-20.3787981885229,22.9734711781954,-13.3529604427561));
#34923=CARTESIAN_POINT('Ctrl Pts',(-20.3946642084834,22.8956528080165,-13.3579619205416));
#34924=CARTESIAN_POINT('Ctrl Pts',(-20.3969160023898,22.8848900702315,-13.3586514288398));
#34925=CARTESIAN_POINT('Ctrl Pts',(-20.399915166782,22.8709124557051,-13.3595438114012));
#34926=CARTESIAN_POINT('Ctrl Pts',(-20.4006124173684,22.8676870754414,-13.3597495176622));
#34927=CARTESIAN_POINT('Ctrl Pts',(-20.4017509648359,22.8624592120358,-13.3600825836484));
#34928=CARTESIAN_POINT('Ctrl Pts',(-20.4021892188173,22.8604560796514,-13.3602101185746));
#34929=CARTESIAN_POINT('Ctrl Pts',(-20.403034349671,22.8566108113337,-13.3604547746606));
#34930=CARTESIAN_POINT('Ctrl Pts',(-20.4034409310714,22.8547686198157,-13.3605719122031));
#34931=CARTESIAN_POINT('Ctrl Pts',(-20.4043796894102,22.8505328484733,-13.3608410832068));
#34932=CARTESIAN_POINT('Ctrl Pts',(-20.4049129819553,22.8481395124083,-13.3609930519314));
#34933=CARTESIAN_POINT('Ctrl Pts',(-20.4066145324135,22.8405440572291,-13.3614749605857));
#34934=CARTESIAN_POINT('Ctrl Pts',(-20.4077929763079,22.8353441928305,-13.3618043146132));
#34935=CARTESIAN_POINT('Ctrl Pts',(-20.4179527689577,22.791024794483,-13.3646068531805));
#34936=CARTESIAN_POINT('Ctrl Pts',(-20.4276518009596,22.7520710986331,-13.3670394681314));
#34937=CARTESIAN_POINT('Ctrl Pts',(-20.4386106719254,22.7113206343329,-13.3695617289842));
#34938=CARTESIAN_POINT('Ctrl Pts',(-20.4391466573235,22.7093351574092,-13.3696845639905));
#34939=CARTESIAN_POINT('Ctrl Pts',(-20.4898449335098,22.5222429794677,-13.3812541286794));
#34940=CARTESIAN_POINT('Ctrl Pts',(-20.5564350762511,22.3419589003215,-13.3919361168441));
#34941=CARTESIAN_POINT('Ctrl Pts',(-20.7177913302788,22.0019177450866,-13.4129665172933));
#34942=CARTESIAN_POINT('Ctrl Pts',(-20.8110778125817,21.8423030256289,-13.4232797042964));
#34943=CARTESIAN_POINT('Ctrl Pts',(-20.9659330079151,21.6229589155487,-13.4389556559534));
#34944=CARTESIAN_POINT('Ctrl Pts',(-21.0170192477865,21.5562878019546,-13.4439427946609));
#34945=CARTESIAN_POINT('Ctrl Pts',(-21.0774445447636,21.4835035223549,-13.4496799656041));
#34946=CARTESIAN_POINT('Ctrl Pts',(-21.0842824636588,21.4753495394669,-13.4503269860015));
#34947=CARTESIAN_POINT('Ctrl Pts',(-21.0965382042667,21.4608811467546,-13.4514828102283));
#34948=CARTESIAN_POINT('Ctrl Pts',(-21.1019403533559,21.4545535408602,-13.4519909694969));
#34949=CARTESIAN_POINT('Ctrl Pts',(-21.1100988159052,21.4450720288827,-13.4527564729705));
#34950=CARTESIAN_POINT('Ctrl Pts',(-21.112836903668,21.441902427445,-13.4530130618698));
#34951=CARTESIAN_POINT('Ctrl Pts',(-21.1177141067322,21.4362787921011,-13.4534695388629));
#34952=CARTESIAN_POINT('Ctrl Pts',(-21.1198507800445,21.4338226400944,-13.453669325197));
#34953=CARTESIAN_POINT('Ctrl Pts',(-21.1241246371097,21.42892475616,-13.4540685621153));
#34954=CARTESIAN_POINT('Ctrl Pts',(-21.1262617945411,21.4264830060158,-13.4542680114774));
#34955=CARTESIAN_POINT('Ctrl Pts',(-21.1314523712772,21.4205706975561,-13.4547519615063));
#34956=CARTESIAN_POINT('Ctrl Pts',(-21.1345095706871,21.4171034800128,-13.455036620311));
#34957=CARTESIAN_POINT('Ctrl Pts',(-21.1459405804623,21.4041954837803,-13.4560995583081));
#34958=CARTESIAN_POINT('Ctrl Pts',(-21.1543622744674,21.3947974336269,-13.456879849679));
#34959=CARTESIAN_POINT('Ctrl Pts',(-21.2998411396458,21.2343587338518,-13.4703117092561));
#34960=CARTESIAN_POINT('Ctrl Pts',(-21.4508490374558,21.096644600442,-13.4835872555689));
#34961=CARTESIAN_POINT('Ctrl Pts',(-21.7248143152441,20.8907090207424,-13.5065469677191));
#34962=CARTESIAN_POINT('Ctrl Pts',(-21.841076787437,20.8145418925604,-13.515990394558));
#34963=CARTESIAN_POINT('Ctrl Pts',(-22.0329889654937,20.7058357148056,-13.5308679535547));
#34964=CARTESIAN_POINT('Ctrl Pts',(-22.1056043664481,20.668275990454,-13.5363460294598));
#34965=CARTESIAN_POINT('Ctrl Pts',(-22.2421358820788,20.604114891618,-13.5462830875753));
#34966=CARTESIAN_POINT('Ctrl Pts',(-22.3056346031707,20.5767320627814,-13.5507663360385));
#34967=CARTESIAN_POINT('Ctrl Pts',(-22.3844495372438,20.5457121219633,-13.5561222276795));
#34968=CARTESIAN_POINT('Ctrl Pts',(-22.3989704858477,20.5401180878865,-13.5571004707037));
#34969=CARTESIAN_POINT('Ctrl Pts',(-22.4170185731768,20.5333149712937,-13.5583052750365));
#34970=CARTESIAN_POINT('Ctrl Pts',(-22.4205077163715,20.5320066668451,-13.5585376836117));
#34971=CARTESIAN_POINT('Ctrl Pts',(-22.4260097043341,20.5299544946848,-13.558903353777));
#34972=CARTESIAN_POINT('Ctrl Pts',(-22.4280210223918,20.5292065858624,-13.5590368581304));
#34973=CARTESIAN_POINT('Ctrl Pts',(-22.4317837347968,20.527811697071,-13.5592862927012));
#34974=CARTESIAN_POINT('Ctrl Pts',(-22.4335349325325,20.5271642345749,-13.5594022513761));
#34975=CARTESIAN_POINT('Ctrl Pts',(-22.4374701215967,20.5257131806889,-13.5596625352809));
#34976=CARTESIAN_POINT('Ctrl Pts',(-22.4396544165787,20.5249104345428,-13.5598068089902));
#34977=CARTESIAN_POINT('Ctrl Pts',(-22.4452128548071,20.5228744944253,-13.5601734389851));
#34978=CARTESIAN_POINT('Ctrl Pts',(-22.4485882041209,20.5216445713151,-13.5603955990214));
#34979=CARTESIAN_POINT('Ctrl Pts',(-22.4672783898046,20.5148695472773,-13.5616231655449));
#34980=CARTESIAN_POINT('Ctrl Pts',(-22.4826333974586,20.5094348349903,-13.5626220588064));
#34981=CARTESIAN_POINT('Ctrl Pts',(-22.7998260673583,20.3998673372801,-13.5830716347356));
#34982=CARTESIAN_POINT('Ctrl Pts',(-23.1154959395728,20.341026147284,-13.6001179677027));
#34983=CARTESIAN_POINT('Ctrl Pts',(-23.5149229875253,20.3266968010335,-13.622764315868));
#34984=CARTESIAN_POINT('Ctrl Pts',(-23.5952100892993,20.3268168806852,-13.6273604802626));
#34985=CARTESIAN_POINT('Ctrl Pts',(-23.7552040523833,20.333034810549,-13.6366885826787));
#34986=CARTESIAN_POINT('Ctrl Pts',(-23.8348541797061,20.3391008204674,-13.641416423137));
#34987=CARTESIAN_POINT('Ctrl Pts',(-23.9295620612457,20.3498648795173,-13.6471718492241));
#34988=CARTESIAN_POINT('Ctrl Pts',(-23.9449188299237,20.3517223468152,-13.6481092699471));
#34989=CARTESIAN_POINT('Ctrl Pts',(-23.9679400159539,20.3546751724777,-13.6495210564125));
#34990=CARTESIAN_POINT('Ctrl Pts',(-23.9756149774831,20.3556877285768,-13.6499928146082));
#34991=CARTESIAN_POINT('Ctrl Pts',(-23.9879571684302,20.3573612975733,-13.6507532312779));
#34992=CARTESIAN_POINT('Ctrl Pts',(-23.9926267578691,20.358004918242,-13.6510413397832));
#34993=CARTESIAN_POINT('Ctrl Pts',(-24.0015456120499,20.3592541704951,-13.6515924131169));
#34994=CARTESIAN_POINT('Ctrl Pts',(-24.0057951149735,20.359858051369,-13.6518553220055));
#34995=CARTESIAN_POINT('Ctrl Pts',(-24.0133224758315,20.360943082111,-13.6523216382853));
#34996=CARTESIAN_POINT('Ctrl Pts',(-24.0166008284844,20.3614208013716,-13.6525249365764));
#34997=CARTESIAN_POINT('Ctrl Pts',(-24.0230571530632,20.362371781726,-13.6529257164081));
#34998=CARTESIAN_POINT('Ctrl Pts',(-24.0262351661336,20.3628447420317,-13.6531231881889));
#34999=CARTESIAN_POINT('Ctrl Pts',(-24.0347616572915,20.364126713324,-13.6536535235515));
#35000=CARTESIAN_POINT('Ctrl Pts',(-24.0401087972791,20.364944436428,-13.6539866634931));
#35001=CARTESIAN_POINT('Ctrl Pts',(-24.0595594134578,20.3679690996865,-13.6552005241912));
#35002=CARTESIAN_POINT('Ctrl Pts',(-24.0736500836644,20.3702562528457,-13.6560837909211));
#35003=CARTESIAN_POINT('Ctrl Pts',(-24.3035629800566,20.4091444781796,-13.6705608880725));
#35004=CARTESIAN_POINT('Ctrl Pts',(-24.5150750082941,20.4675395840331,-13.6848785102126));
#35005=CARTESIAN_POINT('Ctrl Pts',(-24.9777300523539,20.6475808745823,-13.7182518411133));
#35006=CARTESIAN_POINT('Ctrl Pts',(-25.2223737474087,20.7812773116877,-13.737437422956));
#35007=CARTESIAN_POINT('Ctrl Pts',(-25.4561448262258,20.9514404967424,-13.7556547960255));
#35008=CARTESIAN_POINT('Ctrl Pts',(-25.4653930666789,20.9582482546693,-13.7563751053299));
#35009=CARTESIAN_POINT('Ctrl Pts',(-25.477294322151,20.9671074058177,-13.7573013287294));
#35010=CARTESIAN_POINT('Ctrl Pts',(-25.4799806472412,20.9691135962979,-13.7575103462015));
#35011=CARTESIAN_POINT('Ctrl Pts',(-25.484314325226,20.9723606032793,-13.757847457154));
#35012=CARTESIAN_POINT('Ctrl Pts',(-25.4859636173757,20.9735988086236,-13.7579757337333));
#35013=CARTESIAN_POINT('Ctrl Pts',(-25.4891163774683,20.9759704773782,-13.758220905742));
#35014=CARTESIAN_POINT('Ctrl Pts',(-25.4906200296642,20.9771036668868,-13.7583378186949));
#35015=CARTESIAN_POINT('Ctrl Pts',(-25.4940600010956,20.9797008444251,-13.7586052472907));
#35016=CARTESIAN_POINT('Ctrl Pts',(-25.495995657934,20.9811657013581,-13.7587557004781));
#35017=CARTESIAN_POINT('Ctrl Pts',(-25.5011212451101,20.9850537337724,-13.7591540299774));
#35018=CARTESIAN_POINT('Ctrl Pts',(-25.5043083284375,20.9874806820225,-13.7594016407547));
#35019=CARTESIAN_POINT('Ctrl Pts',(-25.5194574151618,20.9990613259702,-13.760578313633));
#35020=CARTESIAN_POINT('Ctrl Pts',(-25.5313599263875,21.0082930605982,-13.7615019546781));
#35021=CARTESIAN_POINT('Ctrl Pts',(-25.7797305223774,21.203736581209,-13.7807678109145));
#35022=CARTESIAN_POINT('Ctrl Pts',(-25.9890676528571,21.4221173260409,-13.7969566667996));
#35023=CARTESIAN_POINT('Ctrl Pts',(-26.238155563539,21.7678591778564,-13.8209895642372));
#35024=CARTESIAN_POINT('Ctrl Pts',(-26.3052669430688,21.8734579261095,-13.8281396498061));
#35025=CARTESIAN_POINT('Ctrl Pts',(-26.3808984994877,22.0093144668135,-13.8372993719535));
#35026=CARTESIAN_POINT('Ctrl Pts',(-26.3953462068264,22.0361559017175,-13.8391069392147));
#35027=CARTESIAN_POINT('Ctrl Pts',(-26.4298910926285,22.1025752984813,-13.8435783690554));
#35028=CARTESIAN_POINT('Ctrl Pts',(-26.4495550181563,22.1423702900796,-13.8462562565726));
#35029=CARTESIAN_POINT('Ctrl Pts',(-26.4716520271938,22.1895168386629,-13.8494319068066));
#35030=CARTESIAN_POINT('Ctrl Pts',(-26.4748889816027,22.196488049649,-13.8499015412386));
#35031=CARTESIAN_POINT('Ctrl Pts',(-26.4798025498354,22.2071699454801,-13.8506212939715));
#35032=CARTESIAN_POINT('Ctrl Pts',(-26.4814971362459,22.2108723727299,-13.8508707910636));
#35033=CARTESIAN_POINT('Ctrl Pts',(-26.4845705231875,22.2176210492361,-13.8513256171017));
#35034=CARTESIAN_POINT('Ctrl Pts',(-26.4859516101013,22.2206662561389,-13.8515308668632));
#35035=CARTESIAN_POINT('Ctrl Pts',(-26.4887153455509,22.2267854127254,-13.8519433431819));
#35036=CARTESIAN_POINT('Ctrl Pts',(-26.4900979158132,22.2298593929863,-13.8521505721173));
#35037=CARTESIAN_POINT('Ctrl Pts',(-26.494008985946,22.2385917860858,-13.8527393166197));
#35038=CARTESIAN_POINT('Ctrl Pts',(-26.4965259790903,22.2442553089449,-13.8531212270297));
#35039=CARTESIAN_POINT('Ctrl Pts',(-26.507067240029,22.2681599181462,-13.8547335253351));
#35040=CARTESIAN_POINT('Ctrl Pts',(-26.514938426467,22.2864676584871,-13.8559691429043));
#35041=CARTESIAN_POINT('Ctrl Pts',(-26.6713083941078,22.6596729741159,-13.8811777876664));
#35042=CARTESIAN_POINT('Ctrl Pts',(-26.7552107178971,23.0382077950116,-13.9076760916674));
#35043=CARTESIAN_POINT('Ctrl Pts',(-26.7721731756054,23.4654090356613,-13.9361761971723));
#35044=CARTESIAN_POINT('Ctrl Pts',(-26.7730191425728,23.5084589201117,-13.9390260147838));
#35045=CARTESIAN_POINT('Ctrl Pts',(-26.7729992036865,23.5593832492775,-13.942361868955));
#35046=CARTESIAN_POINT('Ctrl Pts',(-26.7729673028915,23.5672521628765,-13.9428763340315));
#35047=CARTESIAN_POINT('Ctrl Pts',(-26.7728058495649,23.5881746144899,-13.9442414518283));
#35048=CARTESIAN_POINT('Ctrl Pts',(-26.7726258043491,23.601227751241,-13.9450902466936));
#35049=CARTESIAN_POINT('Ctrl Pts',(-26.7722610364385,23.6195844129097,-13.9462795432568));
#35050=CARTESIAN_POINT('Ctrl Pts',(-26.7721425234256,23.6248889585419,-13.9466227027519));
#35051=CARTESIAN_POINT('Ctrl Pts',(-26.7719494943123,23.6326683905398,-13.9471251916365));
#35052=CARTESIAN_POINT('Ctrl Pts',(-26.7718852260108,23.635143495402,-13.9472849484876));
#35053=CARTESIAN_POINT('Ctrl Pts',(-26.771701091182,23.6419333498852,-13.947722882963));
#35054=CARTESIAN_POINT('Ctrl Pts',(-26.7715754079923,23.6462479529597,-13.9480008132674));
#35055=CARTESIAN_POINT('Ctrl Pts',(-26.7702801209892,23.6878427358036,-13.9506766917176));
#35056=CARTESIAN_POINT('Ctrl Pts',(-26.7684720113068,23.725102241726,-13.9530465914813));
#35057=CARTESIAN_POINT('Ctrl Pts',(-26.7656737502952,23.7675339437805,-13.955708235502));
#35058=CARTESIAN_POINT('Ctrl Pts',(-26.7653174976526,23.7727431846396,-13.9560343583586));
#35059=CARTESIAN_POINT('Ctrl Pts',(-26.7647768149559,23.7803766400378,-13.9565112859884));
#35060=CARTESIAN_POINT('Ctrl Pts',(-26.7646023016556,23.782801514412,-13.9566626463715));
#35061=CARTESIAN_POINT('Ctrl Pts',(-26.7642877251222,23.7871045636001,-13.9569309867099));
#35062=CARTESIAN_POINT('Ctrl Pts',(-26.7641487593398,23.7889828138333,-13.9570480288642));
#35063=CARTESIAN_POINT('Ctrl Pts',(-26.7638543088035,23.7929157271228,-13.9572929241231));
#35064=CARTESIAN_POINT('Ctrl Pts',(-26.7636985003589,23.79497035856,-13.957420758414));
#35065=CARTESIAN_POINT('Ctrl Pts',(-26.7632846177588,23.8003596343954,-13.9577557973066));
#35066=CARTESIAN_POINT('Ctrl Pts',(-26.7630233219941,23.8036940400134,-13.9579628193829));
#35067=CARTESIAN_POINT('Ctrl Pts',(-26.7618479749756,23.8183987414874,-13.9588746166696));
#35068=CARTESIAN_POINT('Ctrl Pts',(-26.7608787358078,23.8297647278527,-13.9595763079363));
#35069=CARTESIAN_POINT('Ctrl Pts',(-26.7532901846323,23.9134995139728,-13.9647246156897));
#35070=CARTESIAN_POINT('Ctrl Pts',(-26.7442845309411,23.985637449347,-13.9690435087567));
#35071=CARTESIAN_POINT('Ctrl Pts',(-26.7201156608629,24.1373041681785,-13.9779927262528));
#35072=CARTESIAN_POINT('Ctrl Pts',(-26.7043806848107,24.216690003693,-13.9826000255598));
#35073=CARTESIAN_POINT('Ctrl Pts',(-26.6079485345692,24.6224540222739,-14.0061193975498));
#35074=CARTESIAN_POINT('Ctrl Pts',(-26.4795488709317,24.9352916931509,-14.0244148164406));
#35075=CARTESIAN_POINT('Ctrl Pts',(-26.2948779216795,25.2394944004927,-14.045944301923));
#35076=CARTESIAN_POINT('Ctrl Pts',(-26.2844878392806,25.2562607023923,-14.0471431511272));
#35077=CARTESIAN_POINT('Ctrl Pts',(-26.2706451959008,25.2781470354461,-14.0487246447038));
#35078=CARTESIAN_POINT('Ctrl Pts',(-26.2673307496776,25.2833542656059,-14.0491021570046));
#35079=CARTESIAN_POINT('Ctrl Pts',(-26.2621860619854,25.2913859029982,-14.0496863657435));
#35080=CARTESIAN_POINT('Ctrl Pts',(-26.2603663091161,25.2942170389813,-14.0498926707855));
#35081=CARTESIAN_POINT('Ctrl Pts',(-26.256729510789,25.2998556603448,-14.050304303584));
#35082=CARTESIAN_POINT('Ctrl Pts',(-26.2549125234928,25.3026631784275,-14.0505096289949));
#35083=CARTESIAN_POINT('Ctrl Pts',(-26.2508689344897,25.3088898609722,-14.0509658366997));
#35084=CARTESIAN_POINT('Ctrl Pts',(-26.2486402054202,25.3123076310078,-14.0512167985272));
#35085=CARTESIAN_POINT('Ctrl Pts',(-26.2421726854089,25.3221845667361,-14.0519436569247));
#35086=CARTESIAN_POINT('Ctrl Pts',(-26.2379171726087,25.3286327011448,-14.0524201816295));
#35087=CARTESIAN_POINT('Ctrl Pts',(-26.2085817857222,25.3727371375646,-14.0556933646411));
#35088=CARTESIAN_POINT('Ctrl Pts',(-26.1827356043435,25.4098753690209,-14.0585189247731));
#35089=CARTESIAN_POINT('Ctrl Pts',(-26.108577587697,25.5117873136047,-14.0664737870782));
#35090=CARTESIAN_POINT('Ctrl Pts',(-26.0586015664174,25.5753029224919,-14.0716661951356));
#35091=CARTESIAN_POINT('Ctrl Pts',(-25.8099939073765,25.8679253920806,-14.0967343797163));
#35092=CARTESIAN_POINT('Ctrl Pts',(-25.5821108278621,26.0700832854051,-14.1177443458217));
#35093=CARTESIAN_POINT('Ctrl Pts',(-25.3069463817119,26.2522643045322,-14.1395136487628));
#35094=CARTESIAN_POINT('Ctrl Pts',(-25.284335421391,26.2668308050833,-14.1412775274237));
#35095=CARTESIAN_POINT('Ctrl Pts',(-25.2547628703622,26.2853624219483,-14.1435498508367));
#35096=CARTESIAN_POINT('Ctrl Pts',(-25.2479657202709,26.2895866730746,-14.1440697920628));
#35097=CARTESIAN_POINT('Ctrl Pts',(-25.2354693414437,26.2972884686461,-14.1450213034697));
#35098=CARTESIAN_POINT('Ctrl Pts',(-25.2297749225072,26.3007736959443,-14.1454532329046));
#35099=CARTESIAN_POINT('Ctrl Pts',(-25.2223330331715,26.3052967217282,-14.1460155083316));
#35100=CARTESIAN_POINT('Ctrl Pts',(-25.2205953959572,26.3063505720964,-14.146146640203));
#35101=CARTESIAN_POINT('Ctrl Pts',(-25.2160321361956,26.3091122186658,-14.1464905976192));
#35102=CARTESIAN_POINT('Ctrl Pts',(-25.2132048765253,26.3108173221266,-14.1467032894843));
#35103=CARTESIAN_POINT('Ctrl Pts',(-25.1773609186585,26.3323595519688,-14.1493945086868));
#35104=CARTESIAN_POINT('Ctrl Pts',(-25.1439919209377,26.3516086789016,-14.151843188912));
#35105=CARTESIAN_POINT('Ctrl Pts',(-25.1061323342117,26.3725526777194,-14.154551484359));
#35106=CARTESIAN_POINT('Ctrl Pts',(-25.1019755301281,26.3748402557614,-14.154847907316));
#35107=CARTESIAN_POINT('Ctrl Pts',(-25.0957056261584,26.3782726997463,-14.1552935913781));
#35108=CARTESIAN_POINT('Ctrl Pts',(-25.0935962958551,26.3794243829286,-14.1554432867409));
#35109=CARTESIAN_POINT('Ctrl Pts',(-25.0899396295782,26.3814155969606,-14.1557023715276));
#35110=CARTESIAN_POINT('Ctrl Pts',(-25.0883928942793,26.3822562192871,-14.1558118312638));
#35111=CARTESIAN_POINT('Ctrl Pts',(-25.0851674600941,26.3840057618148,-14.1560398160448));
#35112=CARTESIAN_POINT('Ctrl Pts',(-25.0834886440861,26.3849144569191,-14.1561583261292));
#35113=CARTESIAN_POINT('Ctrl Pts',(-25.0795419492055,26.3870461581294,-14.1564365686477));
#35114=CARTESIAN_POINT('Ctrl Pts',(-25.0772734027019,26.3882679405871,-14.1565962221835));
#35115=CARTESIAN_POINT('Ctrl Pts',(-25.069807685094,26.3922772464007,-14.1571207272365));
#35116=CARTESIAN_POINT('Ctrl Pts',(-25.0646042883601,26.3950532455602,-14.1574848442081));
#35117=CARTESIAN_POINT('Ctrl Pts',(-25.0522934320256,26.4015777081451,-14.1583429712535));
#35118=CARTESIAN_POINT('Ctrl Pts',(-25.0451794771443,26.4053139249172,-14.1588362226774));
#35119=CARTESIAN_POINT('Ctrl Pts',(-24.8823042252298,26.490079594058,-14.1700711172647));
#35120=CARTESIAN_POINT('Ctrl Pts',(-24.7201677361425,26.5582855019013,-14.1800491480166));
#35121=CARTESIAN_POINT('Ctrl Pts',(-24.2675718147414,26.7065068428227,-14.2067748534045));
#35122=CARTESIAN_POINT('Ctrl Pts',(-23.9702382988431,26.7596267929562,-14.2232975655068));
#35123=CARTESIAN_POINT('Ctrl Pts',(-23.6445422763731,26.7717224917826,-14.2428990824624));
#35124=CARTESIAN_POINT('Ctrl Pts',(-23.6192183555388,26.7723640937979,-14.2444315816337));
#35125=CARTESIAN_POINT('Ctrl Pts',(-23.5845712542195,26.7728332744458,-14.2465407078534));
#35126=CARTESIAN_POINT('Ctrl Pts',(-23.5752520387482,26.772919042528,-14.2471092390029));
#35127=CARTESIAN_POINT('Ctrl Pts',(-23.5614144903551,26.7729863692157,-14.2479552836639));
#35128=CARTESIAN_POINT('Ctrl Pts',(-23.556896299223,26.7729988507274,-14.2482318268449));
#35129=CARTESIAN_POINT('Ctrl Pts',(-23.5491615873628,26.7730039522033,-14.2487057534324));
#35130=CARTESIAN_POINT('Ctrl Pts',(-23.5459450672254,26.7730012581993,-14.248902989566));
#35131=CARTESIAN_POINT('Ctrl Pts',(-23.5396874115666,26.7729866487757,-14.2492870037418));
#35132=CARTESIAN_POINT('Ctrl Pts',(-23.5366462778263,26.7729752440795,-14.2494737655132));
#35133=CARTESIAN_POINT('Ctrl Pts',(-23.5293724543417,26.7729376700925,-14.24992079268));
#35134=CARTESIAN_POINT('Ctrl Pts',(-23.5251397993997,26.7729074665709,-14.2501811844316));
#35135=CARTESIAN_POINT('Ctrl Pts',(-23.5126176743434,26.7727934395002,-14.2509523346288));
#35136=CARTESIAN_POINT('Ctrl Pts',(-23.5043285012374,26.7726859703146,-14.2514638345715));
#35137=CARTESIAN_POINT('Ctrl Pts',(-23.4390418115037,26.7715875716286,-14.2555007015803));
#35138=CARTESIAN_POINT('Ctrl Pts',(-23.3820823961684,26.7691165233904,-14.2590723078735));
#35139=CARTESIAN_POINT('Ctrl Pts',(-23.1845567442088,26.7552903796023,-14.271642038286));
#35140=CARTESIAN_POINT('Ctrl Pts',(-23.0447079933374,26.7362244083592,-14.2808749312802));
#35141=CARTESIAN_POINT('Ctrl Pts',(-22.6672263459862,26.6592794960374,-14.3066071317356));
#35142=CARTESIAN_POINT('Ctrl Pts',(-22.4342138532829,26.5834420348808,-14.323442301079));
#35143=CARTESIAN_POINT('Ctrl Pts',(-22.1959241754897,26.474671252359,-14.3406083269416));
#35144=CARTESIAN_POINT('Ctrl Pts',(-22.1799007748588,26.4671972067472,-14.3417619806383));
#35145=CARTESIAN_POINT('Ctrl Pts',(-22.1340809458916,26.4453638517106,-14.3450574533542));
#35146=CARTESIAN_POINT('Ctrl Pts',(-22.1044429561877,26.4306771938573,-14.3471848573424));
#35147=CARTESIAN_POINT('Ctrl Pts',(-22.0750360145738,26.4155367741587,-14.3492876249023));
#35148=CARTESIAN_POINT('',(-26.7730011641602,23.5472836196309,-14.1857734492732));
#35149=CARTESIAN_POINT('Ctrl Pts',(-22.0750361948364,26.4155368669684,-14.5938261690085));
#35150=CARTESIAN_POINT('Ctrl Pts',(-22.1529748938833,26.4556642779524,-14.5879327433542));
#35151=CARTESIAN_POINT('Ctrl Pts',(-22.2325420634903,26.4926071512902,-14.581991238956));
#35152=CARTESIAN_POINT('Ctrl Pts',(-22.4878132603249,26.5986874494668,-14.5632850366916));
#35153=CARTESIAN_POINT('Ctrl Pts',(-22.6681322416348,26.6556695193257,-14.5505680012588));
#35154=CARTESIAN_POINT('Ctrl Pts',(-22.8638382575462,26.699076082963,-14.5379327783548));
#35155=CARTESIAN_POINT('Ctrl Pts',(-22.8752687559018,26.701546111353,-14.5371990027969));
#35156=CARTESIAN_POINT('Ctrl Pts',(-22.8901593024758,26.7046790875856,-14.5362488006713));
#35157=CARTESIAN_POINT('Ctrl Pts',(-22.8936071581102,26.7053986172831,-14.5360291807727));
#35158=CARTESIAN_POINT('Ctrl Pts',(-22.8989076197223,26.7064957008315,-14.5356921704626));
#35159=CARTESIAN_POINT('Ctrl Pts',(-22.9007593759063,26.7068772762126,-14.5355745488345));
#35160=CARTESIAN_POINT('Ctrl Pts',(-22.9044381328837,26.7076319517035,-14.5353411087892));
#35161=CARTESIAN_POINT('Ctrl Pts',(-22.9062651114416,26.7080050935962,-14.5352252888435));
#35162=CARTESIAN_POINT('Ctrl Pts',(-22.9103349664637,26.70883264135,-14.5349675349158));
#35163=CARTESIAN_POINT('Ctrl Pts',(-22.9125779982417,26.7092862429528,-14.5348256479764));
#35164=CARTESIAN_POINT('Ctrl Pts',(-22.917217760309,26.7102193851504,-14.5345324991033));
#35165=CARTESIAN_POINT('Ctrl Pts',(-22.9196145579069,26.7106985892683,-14.5343812565649));
#35166=CARTESIAN_POINT('Ctrl Pts',(-22.9326310479226,26.7132856465956,-14.533560919835));
#35167=CARTESIAN_POINT('Ctrl Pts',(-22.9432609350784,26.715342734628,-14.5328947107282));
#35168=CARTESIAN_POINT('Ctrl Pts',(-23.04445356753,26.7343969117425,-14.5265862225262));
#35169=CARTESIAN_POINT('Ctrl Pts',(-23.1357054217989,26.7475580080232,-14.5211526117193));
#35170=CARTESIAN_POINT('Ctrl Pts',(-23.3786046763016,26.7720141111179,-14.5070656259211));
#35171=CARTESIAN_POINT('Ctrl Pts',(-23.5307008236378,26.7765249800005,-14.4986228120105));
#35172=CARTESIAN_POINT('Ctrl Pts',(-23.7875013464481,26.7659737404454,-14.484256001229));
#35173=CARTESIAN_POINT('Ctrl Pts',(-23.8921709884389,26.7565339244768,-14.4783700186535));
#35174=CARTESIAN_POINT('Ctrl Pts',(-24.1466701526975,26.7209764347829,-14.4637083241453));
#35175=CARTESIAN_POINT('Ctrl Pts',(-24.2954556135771,26.689339464077,-14.45482767804));
#35176=CARTESIAN_POINT('Ctrl Pts',(-24.4522229871592,26.6442293742173,-14.4449056876568));
#35177=CARTESIAN_POINT('Ctrl Pts',(-24.4629871015457,26.6410710324498,-14.4442215634225));
#35178=CARTESIAN_POINT('Ctrl Pts',(-24.4779465715137,26.6365967543204,-14.4432667543107));
#35179=CARTESIAN_POINT('Ctrl Pts',(-24.4821561426524,26.6353283089849,-14.4429976255283));
#35180=CARTESIAN_POINT('Ctrl Pts',(-24.4894099896754,26.6331263485544,-14.4425330921687));
#35181=CARTESIAN_POINT('Ctrl Pts',(-24.4924555100992,26.6321969258939,-14.4423378220439));
#35182=CARTESIAN_POINT('Ctrl Pts',(-24.4987457200043,26.6302671035853,-14.4419340210756));
#35183=CARTESIAN_POINT('Ctrl Pts',(-24.5019902142863,26.6292660871577,-14.4417254702038));
#35184=CARTESIAN_POINT('Ctrl Pts',(-24.5095508916181,26.626920316326,-14.4412388492059));
#35185=CARTESIAN_POINT('Ctrl Pts',(-24.5138658310568,26.6255716060835,-14.4409606492585));
#35186=CARTESIAN_POINT('Ctrl Pts',(-24.5228954220955,26.6227283789244,-14.4403774638809));
#35187=CARTESIAN_POINT('Ctrl Pts',(-24.5276094963504,26.6212320801872,-14.4400724202754));
#35188=CARTESIAN_POINT('Ctrl Pts',(-24.560537114989,26.6106969974119,-14.4379376196246));
#35189=CARTESIAN_POINT('Ctrl Pts',(-24.5886275212507,26.6012806458792,-14.4360954345587));
#35190=CARTESIAN_POINT('Ctrl Pts',(-24.6670256066189,26.5737922925714,-14.4308932247388));
#35191=CARTESIAN_POINT('Ctrl Pts',(-24.7170174009859,26.5548546647446,-14.4275048550132));
#35192=CARTESIAN_POINT('Ctrl Pts',(-24.8792879911885,26.488723706357,-14.4162663795987));
#35193=CARTESIAN_POINT('Ctrl Pts',(-24.9893557575942,26.4364133924099,-14.4082547827664));
#35194=CARTESIAN_POINT('Ctrl Pts',(-25.1783747031892,26.3330764031351,-14.3938506268614));
#35195=CARTESIAN_POINT('Ctrl Pts',(-25.2585584521191,26.2845861469276,-14.3875191880015));
#35196=CARTESIAN_POINT('Ctrl Pts',(-25.4645677693668,26.1474017314385,-14.3707653515543));
#35197=CARTESIAN_POINT('Ctrl Pts',(-25.5863596408755,26.0530631311435,-14.3603428258114));
#35198=CARTESIAN_POINT('Ctrl Pts',(-25.7049823542067,25.9467679678763,-14.3499454415899));
#35199=CARTESIAN_POINT('Ctrl Pts',(-25.7090032614252,25.9431466228489,-14.3495927060471));
#35200=CARTESIAN_POINT('Ctrl Pts',(-25.7184808567197,25.9345674956429,-14.348760609184));
#35201=CARTESIAN_POINT('Ctrl Pts',(-25.7239297142545,25.9296010611565,-14.348281691453));
#35202=CARTESIAN_POINT('Ctrl Pts',(-25.7321197451101,25.9220845327543,-14.347561105084));
#35203=CARTESIAN_POINT('Ctrl Pts',(-25.7348735618021,25.9195483201717,-14.3473186884582));
#35204=CARTESIAN_POINT('Ctrl Pts',(-25.7411772231156,25.9137224346399,-14.3467635030599));
#35205=CARTESIAN_POINT('Ctrl Pts',(-25.7447240984481,25.9104295438876,-14.3464509141872));
#35206=CARTESIAN_POINT('Ctrl Pts',(-25.7503301009169,25.9052014136746,-14.3459565489124));
#35207=CARTESIAN_POINT('Ctrl Pts',(-25.7523941097658,25.9032714473814,-14.345774468762));
#35208=CARTESIAN_POINT('Ctrl Pts',(-25.7829900701246,25.8745869574742,-14.3430744534272));
#35209=CARTESIAN_POINT('Ctrl Pts',(-25.8110368073388,25.847316362196,-14.3405872370274));
#35210=CARTESIAN_POINT('Ctrl Pts',(-25.8419373361861,25.8161565523279,-14.3378402368675));
#35211=CARTESIAN_POINT('Ctrl Pts',(-25.8452855631034,25.8127652187962,-14.3375424956511));
#35212=CARTESIAN_POINT('Ctrl Pts',(-25.8503147292063,25.8076486537209,-14.3370951588641));
#35213=CARTESIAN_POINT('Ctrl Pts',(-25.8520012583047,25.8059289632343,-14.3369451245644));
#35214=CARTESIAN_POINT('Ctrl Pts',(-25.8549180935857,25.8029480980112,-14.3366856096098));
#35215=CARTESIAN_POINT('Ctrl Pts',(-25.8561492932698,25.8016878053947,-14.336576058096));
#35216=CARTESIAN_POINT('Ctrl Pts',(-25.8587116745477,25.7990605690405,-14.3363480392613));
#35217=CARTESIAN_POINT('Ctrl Pts',(-25.8600426742777,25.7976934542324,-14.3362295866796));
#35218=CARTESIAN_POINT('Ctrl Pts',(-25.8632012504843,25.7944434041925,-14.3359484607114));
#35219=CARTESIAN_POINT('Ctrl Pts',(-25.8650277482358,25.7925594118868,-14.335785872824));
#35220=CARTESIAN_POINT('Ctrl Pts',(-25.8688758974944,25.7885804178831,-14.3354432727126));
#35221=CARTESIAN_POINT('Ctrl Pts',(-25.8708970169311,25.7864849015126,-14.335263302104));
#35222=CARTESIAN_POINT('Ctrl Pts',(-25.8868846540543,25.7698637463973,-14.3338394112749));
#35223=CARTESIAN_POINT('Ctrl Pts',(-25.9007179102175,25.7552097134203,-14.3326057499154));
#35224=CARTESIAN_POINT('Ctrl Pts',(-26.0029332399891,25.6448744280127,-14.323468906908));
#35225=CARTESIAN_POINT('Ctrl Pts',(-26.0855903906801,25.5440313185129,-14.315958498784));
#35226=CARTESIAN_POINT('Ctrl Pts',(-26.187870094986,25.4025625020677,-14.3060774700461));
#35227=CARTESIAN_POINT('Ctrl Pts',(-26.2130739087754,25.3661437935234,-14.3035879545081));
#35228=CARTESIAN_POINT('Ctrl Pts',(-26.2628664158555,25.290928247686,-14.2985325526093));
#35229=CARTESIAN_POINT('Ctrl Pts',(-26.287392209136,25.2521022491927,-14.2959678251093));
#35230=CARTESIAN_POINT('Ctrl Pts',(-26.4468880762129,24.9872377639166,-14.2786921335534));
#35231=CARTESIAN_POINT('Ctrl Pts',(-26.5545299934082,24.745959264001,-14.2639088453605));
#35232=CARTESIAN_POINT('Ctrl Pts',(-26.6363833815997,24.4787873842402,-14.2469685661757));
#35233=CARTESIAN_POINT('Ctrl Pts',(-26.6410170174616,24.4632451240166,-14.2459815744053));
#35234=CARTESIAN_POINT('Ctrl Pts',(-26.647128904575,24.4421645991918,-14.2446406132537));
#35235=CARTESIAN_POINT('Ctrl Pts',(-26.6487100387485,24.4366562102536,-14.2442900083879));
#35236=CARTESIAN_POINT('Ctrl Pts',(-26.6511721334537,24.4279916292927,-14.2437381764648));
#35237=CARTESIAN_POINT('Ctrl Pts',(-26.6520629924532,24.4248382424324,-14.2435372725999));
#35238=CARTESIAN_POINT('Ctrl Pts',(-26.6537664972082,24.4187729792357,-14.2431507145183));
#35239=CARTESIAN_POINT('Ctrl Pts',(-26.6545798584962,24.4158613058583,-14.2429650838459));
#35240=CARTESIAN_POINT('Ctrl Pts',(-26.6564847171522,24.4090050708421,-14.2425278269855));
#35241=CARTESIAN_POINT('Ctrl Pts',(-26.6575727977719,24.4050595726373,-14.2422760898469));
#35242=CARTESIAN_POINT('Ctrl Pts',(-26.6598027881911,24.3969128644017,-14.2417560634275));
#35243=CARTESIAN_POINT('Ctrl Pts',(-26.6609437060333,24.3927113937467,-14.2414877424238));
#35244=CARTESIAN_POINT('Ctrl Pts',(-26.663866378184,24.3818616655537,-14.2407944988928));
#35245=CARTESIAN_POINT('Ctrl Pts',(-26.6656353472703,24.3752100141166,-14.2403691615185));
#35246=CARTESIAN_POINT('Ctrl Pts',(-26.6797216155946,24.3215515487727,-14.2369352616329));
#35247=CARTESIAN_POINT('Ctrl Pts',(-26.6909950379124,24.2742794743362,-14.2338930518393));
#35248=CARTESIAN_POINT('Ctrl Pts',(-26.7491504470632,24.0034163399461,-14.2163531150854));
#35249=CARTESIAN_POINT('Ctrl Pts',(-26.773211034177,23.7756419122829,-14.2011169766266));
#35250=CARTESIAN_POINT('Ctrl Pts',(-26.7730011706773,23.5472907023771,-14.185668766916));
#35251=CARTESIAN_POINT('Ctrl Pts',(-26.7730011641601,23.5472836196309,-14.1857734492732));
#35252=CARTESIAN_POINT('Ctrl Pts',(-26.7728767773161,23.4122619271285,-14.1774340875472));
#35253=CARTESIAN_POINT('Ctrl Pts',(-26.7642634230747,23.2776162714252,-14.1690947258212));
#35254=CARTESIAN_POINT('Ctrl Pts',(-26.7473235194452,23.1442295498557,-14.1607553640952));
#35255=CARTESIAN_POINT('Ctrl Pts',(-26.7336796613005,23.0367962640898,-14.1540386158246));
#35256=CARTESIAN_POINT('Ctrl Pts',(-26.7146351950569,22.9301788636574,-14.1473218675541));
#35257=CARTESIAN_POINT('Ctrl Pts',(-26.6902963387095,22.8248268273487,-14.1406051192835));
#35258=CARTESIAN_POINT('Ctrl Pts',(-26.6679311051526,22.72801772243,-14.1344330279712));
#35259=CARTESIAN_POINT('Ctrl Pts',(-26.6410452778483,22.632073382233,-14.1282609366589));
#35260=CARTESIAN_POINT('Ctrl Pts',(-26.6097205700781,22.5374480665544,-14.1220888453465));
#35261=CARTESIAN_POINT('Ctrl Pts',(-26.5784383041901,22.4429509588235,-14.1159251166077));
#35262=CARTESIAN_POINT('Ctrl Pts',(-26.5427292471014,22.3497697322221,-14.1097613878689));
#35263=CARTESIAN_POINT('Ctrl Pts',(-26.502725916035,22.2583475517289,-14.1035976591301));
#35264=CARTESIAN_POINT('Ctrl Pts',(-26.4627649647434,22.1670222244556,-14.0974404602834));
#35265=CARTESIAN_POINT('Ctrl Pts',(-26.4185189572323,22.0774526341689,-14.0912832614368));
#35266=CARTESIAN_POINT('Ctrl Pts',(-26.3701696101475,21.9900649682432,-14.0851260625901));
#35267=CARTESIAN_POINT('Ctrl Pts',(-26.3218556035036,21.902741177402,-14.0789733642824));
#35268=CARTESIAN_POINT('Ctrl Pts',(-26.2694444300505,21.8175965190385,-14.0728206659747));
#35269=CARTESIAN_POINT('Ctrl Pts',(-26.2131647341598,21.735034593137,-14.066667967667));
#35270=CARTESIAN_POINT('Ctrl Pts',(-26.1569063796098,21.6525039748352,-14.0605176024712));
#35271=CARTESIAN_POINT('Ctrl Pts',(-26.0967826618406,21.5725545015265,-14.0543672372754));
#35272=CARTESIAN_POINT('Ctrl Pts',(-26.033066257837,21.4955619068611,-14.0482168720797));
#35273=CARTESIAN_POINT('Ctrl Pts',(-25.9693569691713,21.4185779101122,-14.0420671937075));
#35274=CARTESIAN_POINT('Ctrl Pts',(-25.9020560688728,21.3445504701877,-14.0359175153353));
#35275=CARTESIAN_POINT('Ctrl Pts',(-25.8314766970087,21.2738224602698,-14.029767836963));
#35276=CARTESIAN_POINT('Ctrl Pts',(-25.7608863249723,21.2030834270136,-14.0236172001306));
#35277=CARTESIAN_POINT('Ctrl Pts',(-25.6870167733329,21.1356451526846,-14.0174665632981));
#35278=CARTESIAN_POINT('Ctrl Pts',(-25.6102174981083,21.0718131235895,-14.0113159264657));
#35279=CARTESIAN_POINT('Ctrl Pts',(-25.5333360637923,21.0079128076322,-14.0051587097439));
#35280=CARTESIAN_POINT('Ctrl Pts',(-25.4535189819524,20.9476267190143,-13.9990014930221));
#35281=CARTESIAN_POINT('Ctrl Pts',(-25.3711481098542,20.8912194638409,-13.9928442763002));
#35282=CARTESIAN_POINT('Ctrl Pts',(-25.2887312833839,20.8347807392909,-13.9866836244924));
#35283=CARTESIAN_POINT('Ctrl Pts',(-25.2037581987513,20.7822253862395,-13.9805229726846));
#35284=CARTESIAN_POINT('Ctrl Pts',(-25.1166371570558,20.7337730327575,-13.9743623208768));
#35285=CARTESIAN_POINT('Ctrl Pts',(-25.0293703308769,20.6852396012582,-13.9681913601078));
#35286=CARTESIAN_POINT('Ctrl Pts',(-24.9399487573529,20.6408230768919,-13.9620203993388));
#35287=CARTESIAN_POINT('Ctrl Pts',(-24.8488027644645,20.6006958098337,-13.9558494385697));
#35288=CARTESIAN_POINT('Ctrl Pts',(-24.7792293167448,20.5700659134627,-13.9511390283494));
#35289=CARTESIAN_POINT('Ctrl Pts',(-24.7086515831127,20.5419341992923,-13.946428618129));
#35290=CARTESIAN_POINT('Ctrl Pts',(-24.6372665088554,20.5163576462448,-13.9417182079087));
#35291=CARTESIAN_POINT('Ctrl Pts',(-24.5437300277332,20.4828444672477,-13.9355461165964));
#35292=CARTESIAN_POINT('Ctrl Pts',(-24.4484775151185,20.45360198161,-13.929374025284));
#35293=CARTESIAN_POINT('Ctrl Pts',(-24.3519353168928,20.4288069892546,-13.9232019339717));
#35294=CARTESIAN_POINT('Ctrl Pts',(-24.2555239238012,20.4040455916624,-13.9170382052329));
#35295=CARTESIAN_POINT('Ctrl Pts',(-24.1578267352732,20.3837198173159,-13.9108744764941));
#35296=CARTESIAN_POINT('Ctrl Pts',(-24.0592882246176,20.3679577267099,-13.9047107477554));
#35297=CARTESIAN_POINT('Ctrl Pts',(-23.9608541062657,20.3522123345595,-13.8985535489087));
#35298=CARTESIAN_POINT('Ctrl Pts',(-23.8615808643558,20.3410210823747,-13.892396350062));
#35299=CARTESIAN_POINT('Ctrl Pts',(-23.7619252830272,20.3344614612353,-13.8862391512153));
#35300=CARTESIAN_POINT('Ctrl Pts',(-23.6623425438852,20.3279066347812,-13.8800864529076));
#35301=CARTESIAN_POINT('Ctrl Pts',(-23.5623784531072,20.3259767369911,-13.8739337545999));
#35302=CARTESIAN_POINT('Ctrl Pts',(-23.4624961581072,20.3286975684203,-13.8677810562922));
#35303=CARTESIAN_POINT('Ctrl Pts',(-23.3626517386156,20.3314173681063,-13.8616306910965));
#35304=CARTESIAN_POINT('Ctrl Pts',(-23.2628894870293,20.338784381014,-13.8554803259007));
#35305=CARTESIAN_POINT('Ctrl Pts',(-23.1636729078426,20.3507722993873,-13.849329960705));
#35306=CARTESIAN_POINT('Ctrl Pts',(-23.064467408369,20.3627588790458,-13.8431802823328));
#35307=CARTESIAN_POINT('Ctrl Pts',(-22.9658078914109,20.3793652861328,-13.8370306039605));
#35308=CARTESIAN_POINT('Ctrl Pts',(-22.8681520874105,20.4005134081464,-13.8308809255883));
#35309=CARTESIAN_POINT('Ctrl Pts',(-22.7704810632311,20.4216648262077,-13.8247302887559));
#35310=CARTESIAN_POINT('Ctrl Pts',(-22.6738144873285,20.4473592732172,-13.8185796519234));
#35311=CARTESIAN_POINT('Ctrl Pts',(-22.57859826625,20.4774678742631,-13.812429015091));
#35312=CARTESIAN_POINT('Ctrl Pts',(-22.4832801838168,20.5076086851872,-13.8062717983692));
#35313=CARTESIAN_POINT('Ctrl Pts',(-22.3894159695468,20.542172948723,-13.8001145816474));
#35314=CARTESIAN_POINT('Ctrl Pts',(-22.2974346510364,20.5809824327635,-13.7939573649256));
#35315=CARTESIAN_POINT('Ctrl Pts',(-22.2054020165251,20.6198135684562,-13.7877967131178));
#35316=CARTESIAN_POINT('Ctrl Pts',(-22.1152547617075,20.662894453953,-13.7816360613099));
#35317=CARTESIAN_POINT('Ctrl Pts',(-22.0273983674179,20.7100002969717,-13.7754754095021));
#35318=CARTESIAN_POINT('Ctrl Pts',(-21.9393949581386,20.7571849648167,-13.7693044487331));
#35319=CARTESIAN_POINT('Ctrl Pts',(-21.8536904396184,20.8084078205895,-13.7631334879641));
#35320=CARTESIAN_POINT('Ctrl Pts',(-21.7706624234681,20.8633999847159,-13.756962527195));
#35321=CARTESIAN_POINT('Ctrl Pts',(-21.7072855798137,20.9053765361217,-13.7522521169746));
#35322=CARTESIAN_POINT('Ctrl Pts',(-21.6454676396496,20.9495483835006,-13.7475417067542));
#35323=CARTESIAN_POINT('Ctrl Pts',(-21.5853629975758,20.9957806330013,-13.7428312965338));
#35324=CARTESIAN_POINT('Ctrl Pts',(-21.5066073644536,21.0563591499753,-13.7366592052214));
#35325=CARTESIAN_POINT('Ctrl Pts',(-21.4305171495401,21.1206898838442,-13.7304871139091));
#35326=CARTESIAN_POINT('Ctrl Pts',(-21.3574715555996,21.188509710518,-13.7243150225968));
#35327=CARTESIAN_POINT('Ctrl Pts',(-21.2845249312174,21.2562376480314,-13.718151293858));
#35328=CARTESIAN_POINT('Ctrl Pts',(-21.2146150441517,21.3274449892226,-13.7119875651192));
#35329=CARTESIAN_POINT('Ctrl Pts',(-21.1480898905112,21.4018270133658,-13.7058238363804));
#35330=CARTESIAN_POINT('Ctrl Pts',(-21.0816352140273,21.4761302367355,-13.6996666375337));
#35331=CARTESIAN_POINT('Ctrl Pts',(-21.0185584300508,21.5536011345486,-13.693509438687));
#35332=CARTESIAN_POINT('Ctrl Pts',(-20.9591716443192,21.6338972938586,-13.6873522398404));
#35333=CARTESIAN_POINT('Ctrl Pts',(-20.8998282667267,21.7141347615454,-13.6811995415327));
#35334=CARTESIAN_POINT('Ctrl Pts',(-20.8441697824914,21.7971930367696,-13.6750468432249));
#35335=CARTESIAN_POINT('Ctrl Pts',(-20.792468248865,21.8826964121347,-13.6688941449172));
#35336=CARTESIAN_POINT('Ctrl Pts',(-20.7407863205338,21.9681673644981,-13.6627437797215));
#35337=CARTESIAN_POINT('Ctrl Pts',(-20.6930585858942,22.0560812033799,-13.6565934145257));
#35338=CARTESIAN_POINT('Ctrl Pts',(-20.6495134556182,22.1460337542148,-13.65044304933));
#35339=CARTESIAN_POINT('Ctrl Pts',(-20.6059731881137,22.235976259869,-13.6442933709578));
#35340=CARTESIAN_POINT('Ctrl Pts',(-20.5666147856328,22.3279566338457,-13.6381436925856));
#35341=CARTESIAN_POINT('Ctrl Pts',(-20.5316199535256,22.4215475567254,-13.6319940142133));
#35342=CARTESIAN_POINT('Ctrl Pts',(-20.4966196672868,22.5151530662506,-13.6258433773809));
#35343=CARTESIAN_POINT('Ctrl Pts',(-20.4659844544014,22.6103692163269,-13.6196927405484));
#35344=CARTESIAN_POINT('Ctrl Pts',(-20.4398469216358,22.7067511959412,-13.613542103716));
#35345=CARTESIAN_POINT('Ctrl Pts',(-20.4136814272008,22.8032362840269,-13.6073848869941));
#35346=CARTESIAN_POINT('Ctrl Pts',(-20.3920233350419,22.9008892720935,-13.6012276702723));
#35347=CARTESIAN_POINT('Ctrl Pts',(-20.3749546031006,22.9992528700164,-13.5950704535505));
#35348=CARTESIAN_POINT('Ctrl Pts',(-20.3578763485836,23.0976713445877,-13.5889098017427));
#35349=CARTESIAN_POINT('Ctrl Pts',(-20.3453926075317,23.1968007875181,-13.5827491499349));
#35350=CARTESIAN_POINT('Ctrl Pts',(-20.3375334380064,23.2961785512203,-13.5765884981271));
#35351=CARTESIAN_POINT('Ctrl Pts',(-20.3296611172957,23.3957226092603,-13.570417537358));
#35352=CARTESIAN_POINT('Ctrl Pts',(-20.3264288397547,23.4955153836992,-13.564246576589));
#35353=CARTESIAN_POINT('Ctrl Pts',(-20.3278145075697,23.5950938427448,-13.55807561582));
#35354=CARTESIAN_POINT('Ctrl Pts',(-20.3288722138301,23.6711039502095,-13.5533652055996));
#35355=CARTESIAN_POINT('Ctrl Pts',(-20.332619512849,23.746989176551,-13.5486547953793));
#35356=CARTESIAN_POINT('Ctrl Pts',(-20.3390263729923,23.8225467111563,-13.5439443851589));
#35357=CARTESIAN_POINT('Ctrl Pts',(-20.3474213373331,23.9215504032133,-13.5377722938466));
#35358=CARTESIAN_POINT('Ctrl Pts',(-20.36041387624,24.0203398665099,-13.5316002025343));
#35359=CARTESIAN_POINT('Ctrl Pts',(-20.377987594171,24.1184538416727,-13.5254281112219));
#35360=CARTESIAN_POINT('Ctrl Pts',(-20.3955375014517,24.2164348820989,-13.5192643824831));
#35361=CARTESIAN_POINT('Ctrl Pts',(-20.4176561746807,24.3137418296599,-13.5131006537444));
#35362=CARTESIAN_POINT('Ctrl Pts',(-20.4442753538481,24.4099171949202,-13.5069369250056));
#35363=CARTESIAN_POINT('Ctrl Pts',(-20.4708663324936,24.5059906714076,-13.5007797261589));
#35364=CARTESIAN_POINT('Ctrl Pts',(-20.5019482228957,24.6009345325774,-13.4946225273122));
#35365=CARTESIAN_POINT('Ctrl Pts',(-20.5374016536794,24.6943011099223,-13.4884653284655));
#35366=CARTESIAN_POINT('Ctrl Pts',(-20.5728291701553,24.7875994419611,-13.4823126301578));
#35367=CARTESIAN_POINT('Ctrl Pts',(-20.6126217204138,24.8793223774489,-13.4761599318501));
#35368=CARTESIAN_POINT('Ctrl Pts',(-20.6566102739965,24.96903794428,-13.4700072335424));
#35369=CARTESIAN_POINT('Ctrl Pts',(-20.700582147057,25.0587194908404,-13.4638568683467));
#35370=CARTESIAN_POINT('Ctrl Pts',(-20.7487466708534,25.1463947916281,-13.4577065031509));
#35371=CARTESIAN_POINT('Ctrl Pts',(-20.8008872721935,25.2316532074257,-13.4515561379552));
#35372=CARTESIAN_POINT('Ctrl Pts',(-20.8530220508887,25.3169021022462,-13.445406459583));
#35373=CARTESIAN_POINT('Ctrl Pts',(-20.9091317977227,25.3997342780776,-13.4392567812108));
#35374=CARTESIAN_POINT('Ctrl Pts',(-20.9689552211427,25.4797658788986,-13.4331071028386));
#35375=CARTESIAN_POINT('Ctrl Pts',(-21.0287879683631,25.5598099530723,-13.4269564660061));
#35376=CARTESIAN_POINT('Ctrl Pts',(-21.0923352816988,25.6370522372933,-13.4208058291737));
#35377=CARTESIAN_POINT('Ctrl Pts',(-21.1592946137603,25.7111407280545,-13.4146551923412));
#35378=CARTESIAN_POINT('Ctrl Pts',(-21.2263255782413,25.7853084779374,-13.4084979756194));
#35379=CARTESIAN_POINT('Ctrl Pts',(-21.296775558584,25.8563153741095,-13.4023407588976));
#35380=CARTESIAN_POINT('Ctrl Pts',(-21.370304130676,25.9238452792813,-13.3961835421757));
#35381=CARTESIAN_POINT('Ctrl Pts',(-21.4438737240572,25.9914128591106,-13.3900228903679));
#35382=CARTESIAN_POINT('Ctrl Pts',(-21.5205249963508,26.0554993062122,-13.3838622385601));
#35383=CARTESIAN_POINT('Ctrl Pts',(-21.5998849620357,26.1158292516003,-13.3777015867523));
#35384=CARTESIAN_POINT('Ctrl Pts',(-21.679377725164,26.1762601504407,-13.3715306259833));
#35385=CARTESIAN_POINT('Ctrl Pts',(-21.7615878776102,26.2329217448682,-13.3653596652142));
#35386=CARTESIAN_POINT('Ctrl Pts',(-21.8461139181537,26.285582337831,-13.3591887044452));
#35387=CARTESIAN_POINT('Ctrl Pts',(-21.910634231954,26.3257791571901,-13.3544782942248));
#35388=CARTESIAN_POINT('Ctrl Pts',(-21.9765033200759,26.3636456734935,-13.3497678840044));
#35389=CARTESIAN_POINT('Ctrl Pts',(-22.0435343211767,26.3990975251249,-13.345057473784));
#35390=CARTESIAN_POINT('Ctrl Pts',(-22.0540023958228,26.4046339578668,-13.3443218600383));
#35391=CARTESIAN_POINT('Ctrl Pts',(-22.0645031770524,26.41011385114,-13.3435862462925));
#35392=CARTESIAN_POINT('Ctrl Pts',(-22.0750360153462,26.4155367745563,-13.3428506325468));
#35393=CARTESIAN_POINT('Origin',(-23.5502525316942,23.5502525316942,-77.3107734492734));
#35394=CARTESIAN_POINT('',(-22.075036015346,26.4155367745563,-11.8463751360594));
#35395=CARTESIAN_POINT('',(-22.0750360352296,26.4155367847935,-12.0938589134715));
#35396=CARTESIAN_POINT('',(-22.0750360153461,26.4155367745563,-77.3107734492734));
#35397=CARTESIAN_POINT('',(-26.7730017570585,23.5524870146403,-12.689226550727));
#35398=CARTESIAN_POINT('Ctrl Pts',(-26.7730017570585,23.5524870146403,-12.689226550727));
#35399=CARTESIAN_POINT('Ctrl Pts',(-26.7730713768293,23.4520758376819,-12.683051009313));
#35400=CARTESIAN_POINT('Ctrl Pts',(-26.7684439056258,23.3516314719299,-12.6768754678991));
#35401=CARTESIAN_POINT('Ctrl Pts',(-26.7591366801023,23.2516221839477,-12.6706999264851));
#35402=CARTESIAN_POINT('Ctrl Pts',(-26.7498294620169,23.1516129758906,-12.6645243900065));
#35403=CARTESIAN_POINT('Ctrl Pts',(-26.7358425367357,23.0520392722014,-12.6583488535278));
#35404=CARTESIAN_POINT('Ctrl Pts',(-26.7172451528587,22.9533645187556,-12.6521733170492));
#35405=CARTESIAN_POINT('Ctrl Pts',(-26.6986429662274,22.8546642826618,-12.645996185745));
#35406=CARTESIAN_POINT('Ctrl Pts',(-26.6754280335397,22.7568638799424,-12.6398190544408));
#35407=CARTESIAN_POINT('Ctrl Pts',(-26.6477205945032,22.6604159386175,-12.6336419231366));
#35408=CARTESIAN_POINT('Ctrl Pts',(-26.6199790275691,22.5638492001183,-12.627457183316));
#35409=CARTESIAN_POINT('Ctrl Pts',(-26.5877340220277,22.4686386631177,-12.6212724434954));
#35410=CARTESIAN_POINT('Ctrl Pts',(-26.5511555595458,22.3752212215023,-12.6150877036747));
#35411=CARTESIAN_POINT('Ctrl Pts',(-26.5145540442593,22.2817449055144,-12.6088990660523));
#35412=CARTESIAN_POINT('Ctrl Pts',(-26.4736138075433,22.1900643273661,-12.6027104284298));
#35413=CARTESIAN_POINT('Ctrl Pts',(-26.4285519111379,22.1005938667685,-12.5965217908074));
#35414=CARTESIAN_POINT('Ctrl Pts',(-26.383407128174,22.010958834789,-12.5903217698452));
#35415=CARTESIAN_POINT('Ctrl Pts',(-26.3341257493065,21.9235424166777,-12.584121748883));
#35416=CARTESIAN_POINT('Ctrl Pts',(-26.2809696583642,21.8387322903266,-12.5779217279209));
#35417=CARTESIAN_POINT('Ctrl Pts',(-26.2348935038113,21.7652181469775,-12.5725474966894));
#35418=CARTESIAN_POINT('Ctrl Pts',(-26.185906855583,21.6936619245205,-12.567173265458));
#35419=CARTESIAN_POINT('Ctrl Pts',(-26.13420441032,21.6242955613944,-12.5617990342266));
#35420=CARTESIAN_POINT('Ctrl Pts',(-26.0748262035605,21.5446310458982,-12.5556269429142));
#35421=CARTESIAN_POINT('Ctrl Pts',(-26.0116558225816,21.4675747866283,-12.5494548516019));
#35422=CARTESIAN_POINT('Ctrl Pts',(-25.9449506153437,21.393509929837,-12.5432827602896));
#35423=CARTESIAN_POINT('Ctrl Pts',(-25.8783357870669,21.3195454236045,-12.5371190315508));
#35424=CARTESIAN_POINT('Ctrl Pts',(-25.8081959400041,21.2485645839149,-12.530955302812));
#35425=CARTESIAN_POINT('Ctrl Pts',(-25.7348304868387,21.1809199842461,-12.5247915740732));
#35426=CARTESIAN_POINT('Ctrl Pts',(-25.6615427574853,21.113347047682,-12.5186343752265));
#35427=CARTESIAN_POINT('Ctrl Pts',(-25.5850365333912,21.0491036172036,-12.5124771763799));
#35428=CARTESIAN_POINT('Ctrl Pts',(-25.5056494589671,20.9885069511746,-12.5063199775332));
#35429=CARTESIAN_POINT('Ctrl Pts',(-25.4263204116803,20.9279545776338,-12.5001672792255));
#35430=CARTESIAN_POINT('Ctrl Pts',(-25.3441150448641,20.87104393173,-12.4940145809178));
#35431=CARTESIAN_POINT('Ctrl Pts',(-25.2594049003968,20.8180527324375,-12.4878618826101));
#35432=CARTESIAN_POINT('Ctrl Pts',(-25.1747268781368,20.7650816274832,-12.4817115174143));
#35433=CARTESIAN_POINT('Ctrl Pts',(-25.0875463333687,20.7160272460816,-12.4755611522186));
#35434=CARTESIAN_POINT('Ctrl Pts',(-24.9982639332319,20.6711240969909,-12.4694107870228));
#35435=CARTESIAN_POINT('Ctrl Pts',(-24.9089915034387,20.6262259623244,-12.4632611086506));
#35436=CARTESIAN_POINT('Ctrl Pts',(-24.8176180730134,20.5854783334969,-12.4571114302784));
#35437=CARTESIAN_POINT('Ctrl Pts',(-24.7245681590013,20.5490693700124,-12.4509617519062));
#35438=CARTESIAN_POINT('Ctrl Pts',(-24.6315037426627,20.5126547319963,-12.4448111150737));
#35439=CARTESIAN_POINT('Ctrl Pts',(-24.5367627283256,20.4805802607415,-12.4386604782413));
#35440=CARTESIAN_POINT('Ctrl Pts',(-24.4407878665935,20.4529852878491,-12.4325098414088));
#35441=CARTESIAN_POINT('Ctrl Pts',(-24.3447103319206,20.4253607941325,-12.426352624687));
#35442=CARTESIAN_POINT('Ctrl Pts',(-24.2473967323311,20.4022254884456,-12.4201954079652));
#35443=CARTESIAN_POINT('Ctrl Pts',(-24.1493030635705,20.3836682484706,-12.4140381912434));
#35444=CARTESIAN_POINT('Ctrl Pts',(-24.0511546687539,20.3651006554875,-12.4078775394356));
#35445=CARTESIAN_POINT('Ctrl Pts',(-23.9522257682191,20.3511162754397,-12.4017168876277));
#35446=CARTESIAN_POINT('Ctrl Pts',(-23.8529785009793,20.3417521732681,-12.3955562358199));
#35447=CARTESIAN_POINT('Ctrl Pts',(-23.7535651577685,20.3323724016236,-12.3893852750509));
#35448=CARTESIAN_POINT('Ctrl Pts',(-23.6538328178349,20.327628371727,-12.3832143142819));
#35449=CARTESIAN_POINT('Ctrl Pts',(-23.5542447946509,20.3275050044534,-12.3770433535128));
#35450=CARTESIAN_POINT('Ctrl Pts',(-23.4782273866993,20.3274108358972,-12.3723329432924));
#35451=CARTESIAN_POINT('Ctrl Pts',(-23.4022940911173,20.3300078435913,-12.3676225330721));
#35452=CARTESIAN_POINT('Ctrl Pts',(-23.326648150292,20.3352690724649,-12.3629121228517));
#35453=CARTESIAN_POINT('Ctrl Pts',(-23.2275286187997,20.3421629062296,-12.3567400315394));
#35454=CARTESIAN_POINT('Ctrl Pts',(-23.1285536261054,20.3536570328534,-12.350567940227));
#35455=CARTESIAN_POINT('Ctrl Pts',(-23.0301846270619,20.3697420479713,-12.3443958489147));
#35456=CARTESIAN_POINT('Ctrl Pts',(-22.9319489082871,20.3858052694839,-12.3382321201759));
#35457=CARTESIAN_POINT('Ctrl Pts',(-22.8343179761455,20.4064469466979,-12.3320683914372));
#35458=CARTESIAN_POINT('Ctrl Pts',(-22.7377503018681,20.4316057596106,-12.3259046626984));
#35459=CARTESIAN_POINT('Ctrl Pts',(-22.6412849319784,20.4567379191222,-12.3197474638517));
#35460=CARTESIAN_POINT('Ctrl Pts',(-22.5458809985728,20.486377591447,-12.313590265005));
#35461=CARTESIAN_POINT('Ctrl Pts',(-22.4519879275536,20.5204122022722,-12.3074330661583));
#35462=CARTESIAN_POINT('Ctrl Pts',(-22.3581634866755,20.5544219358608,-12.3012803678506));
#35463=CARTESIAN_POINT('Ctrl Pts',(-22.2658481197188,20.5928200735007,-12.2951276695429));
#35464=CARTESIAN_POINT('Ctrl Pts',(-22.1754763104521,20.6354441496548,-12.2889749712352));
#35465=CARTESIAN_POINT('Ctrl Pts',(-22.085138770304,20.6780520626985,-12.2828246060394));
#35466=CARTESIAN_POINT('Ctrl Pts',(-21.9967437158916,20.7248825450383,-12.2766742408437));
#35467=CARTESIAN_POINT('Ctrl Pts',(-21.9107050209418,20.7757252706125,-12.270523875648));
#35468=CARTESIAN_POINT('Ctrl Pts',(-21.8246759341047,20.8265623184781,-12.2643741972757));
#35469=CARTESIAN_POINT('Ctrl Pts',(-21.7410030575587,20.8814104977851,-12.2582245189035));
#35470=CARTESIAN_POINT('Ctrl Pts',(-21.6600741625112,20.940014363409,-12.2520748405313));
#35471=CARTESIAN_POINT('Ctrl Pts',(-21.5791326542628,20.9986273627587,-12.2459242036988));
#35472=CARTESIAN_POINT('Ctrl Pts',(-21.5009363288369,21.0609969562621,-12.2397735668664));
#35473=CARTESIAN_POINT('Ctrl Pts',(-21.4258417337178,21.1268259650449,-12.2336229300339));
#35474=CARTESIAN_POINT('Ctrl Pts',(-21.3506668031569,21.1927253970387,-12.2274657133121));
#35475=CARTESIAN_POINT('Ctrl Pts',(-21.2786005563182,21.2620913476259,-12.2213084965903));
#35476=CARTESIAN_POINT('Ctrl Pts',(-21.2099642525184,21.3345882220903,-12.2151512798685));
#35477=CARTESIAN_POINT('Ctrl Pts',(-21.1412896568058,21.4071255422641,-12.2089906280607));
#35478=CARTESIAN_POINT('Ctrl Pts',(-21.0760490986054,21.4827969358819,-12.2028299762528));
#35479=CARTESIAN_POINT('Ctrl Pts',(-21.0145235670017,21.5612336328097,-12.196669324445));
#35480=CARTESIAN_POINT('Ctrl Pts',(-20.9528950813049,21.639801582224,-12.190498363676));
#35481=CARTESIAN_POINT('Ctrl Pts',(-20.8949942916683,21.7211437238712,-12.184327402907));
#35482=CARTESIAN_POINT('Ctrl Pts',(-20.8410589523442,21.8048621134471,-12.1781564421379));
#35483=CARTESIAN_POINT('Ctrl Pts',(-20.7998890951534,21.8687659320989,-12.1734460319175));
#35484=CARTESIAN_POINT('Ctrl Pts',(-20.7610288359968,21.9340536804532,-12.1687356216972));
#35485=CARTESIAN_POINT('Ctrl Pts',(-20.7245653582472,22.0005397969213,-12.1640252114768));
#35486=CARTESIAN_POINT('Ctrl Pts',(-20.6767869475132,22.0876571312179,-12.1578531201645));
#35487=CARTESIAN_POINT('Ctrl Pts',(-20.6329569696939,22.1771395159093,-12.1516810288521));
#35488=CARTESIAN_POINT('Ctrl Pts',(-20.5933169486501,22.2685936378275,-12.1455089375398));
#35489=CARTESIAN_POINT('Ctrl Pts',(-20.553730635916,22.3599238484516,-12.139345208801));
#35490=CARTESIAN_POINT('Ctrl Pts',(-20.5183231675958,22.4532200913351,-12.1331814800623));
#35491=CARTESIAN_POINT('Ctrl Pts',(-20.4872907772788,22.5480635008778,-12.1270177513235));
#35492=CARTESIAN_POINT('Ctrl Pts',(-20.4562912628667,22.6428064327301,-12.1208605524768));
#35493=CARTESIAN_POINT('Ctrl Pts',(-20.4296577460297,22.7390928620219,-12.1147033536301));
#35494=CARTESIAN_POINT('Ctrl Pts',(-20.4075384498623,22.8364838280126,-12.1085461547834));
#35495=CARTESIAN_POINT('Ctrl Pts',(-20.3854353215592,22.9338036071125,-12.1023934564757));
#35496=CARTESIAN_POINT('Ctrl Pts',(-20.3678399496428,23.0322258954301,-12.0962407581679));
#35497=CARTESIAN_POINT('Ctrl Pts',(-20.3548505060269,23.1312973349708,-12.0900880598602));
#35498=CARTESIAN_POINT('Ctrl Pts',(-20.3418659880266,23.2303312064806,-12.0839376946645));
#35499=CARTESIAN_POINT('Ctrl Pts',(-20.3334839843102,23.3300133098615,-12.0777873294687));
#35500=CARTESIAN_POINT('Ctrl Pts',(-20.3297512603281,23.42988175605,-12.071636964273));
#35501=CARTESIAN_POINT('Ctrl Pts',(-20.3260189531867,23.5297390497301,-12.0654872859008));
#35502=CARTESIAN_POINT('Ctrl Pts',(-20.3269349097758,23.6297822107471,-12.0593376075286));
#35503=CARTESIAN_POINT('Ctrl Pts',(-20.3324938266029,23.7295469217595,-12.0531879291564));
#35504=CARTESIAN_POINT('Ctrl Pts',(-20.3380536098168,23.8293271816354,-12.0470372923239));
#35505=CARTESIAN_POINT('Ctrl Pts',(-20.3482577664134,23.9288284715368,-12.0408866554914));
#35506=CARTESIAN_POINT('Ctrl Pts',(-20.3630490038501,24.0275901843031,-12.034736018659));
#35507=CARTESIAN_POINT('Ctrl Pts',(-20.3778560648037,24.1264575513552,-12.0285788019372));
#35508=CARTESIAN_POINT('Ctrl Pts',(-20.3972599413504,24.2245833308896,-12.0224215852153));
#35509=CARTESIAN_POINT('Ctrl Pts',(-20.4211519463045,24.3215158388819,-12.0162643684935));
#35510=CARTESIAN_POINT('Ctrl Pts',(-20.4450572805103,24.4185024251232,-12.0101037166857));
#35511=CARTESIAN_POINT('Ctrl Pts',(-20.4734556061434,24.5142939975477,-12.003943064878));
#35512=CARTESIAN_POINT('Ctrl Pts',(-20.5061885572147,24.6084548194333,-11.9977824130702));
#35513=CARTESIAN_POINT('Ctrl Pts',(-20.5389762821533,24.7027732058582,-11.9916114523011));
#35514=CARTESIAN_POINT('Ctrl Pts',(-20.5761129593124,24.7954549875517,-11.9854404915321));
#35515=CARTESIAN_POINT('Ctrl Pts',(-20.6173923077243,24.8860850321056,-11.979269530763));
#35516=CARTESIAN_POINT('Ctrl Pts',(-20.6489016094245,24.9552646467752,-11.9745591205426));
#35517=CARTESIAN_POINT('Ctrl Pts',(-20.6828236700518,25.0232492305408,-11.9698487103222));
#35518=CARTESIAN_POINT('Ctrl Pts',(-20.719049499837,25.0898651306627,-11.9651383001018));
#35519=CARTESIAN_POINT('Ctrl Pts',(-20.7665108309347,25.1771420629181,-11.9589669483232));
#35520=CARTESIAN_POINT('Ctrl Pts',(-20.8180952248085,25.2623760123839,-11.9527955965446));
#35521=CARTESIAN_POINT('Ctrl Pts',(-20.8736024092598,25.345151326772,-11.946624244766));
#35522=CARTESIAN_POINT('Ctrl Pts',(-20.9290384121267,25.4278204913332,-11.9404608070367));
#35523=CARTESIAN_POINT('Ctrl Pts',(-20.9883869704736,25.5080369280774,-11.9342973693074));
#35524=CARTESIAN_POINT('Ctrl Pts',(-21.051401799618,25.5854091795477,-11.9281339315781));
#35525=CARTESIAN_POINT('Ctrl Pts',(-21.114352687096,25.6627029207568,-11.9219767479399));
#35526=CARTESIAN_POINT('Ctrl Pts',(-21.1809621784385,25.7371578779558,-11.9158195643017));
#35527=CARTESIAN_POINT('Ctrl Pts',(-21.2509410986799,25.8084120691295,-11.9096623806635));
#35528=CARTESIAN_POINT('Ctrl Pts',(-21.3208667543957,25.8796120251038,-11.9035098835718));
#35529=CARTESIAN_POINT('Ctrl Pts',(-21.3941564353851,25.9476157509724,-11.8973573864801));
#35530=CARTESIAN_POINT('Ctrl Pts',(-21.4704818292711,26.0120956192696,-11.8912048893884));
#35531=CARTESIAN_POINT('Ctrl Pts',(-21.5467735089542,26.0765470057305,-11.8850551099576));
#35532=CARTESIAN_POINT('Ctrl Pts',(-21.626097903105,26.1374773506302,-11.8789053305267));
#35533=CARTESIAN_POINT('Ctrl Pts',(-21.7080918074273,26.1945977112176,-11.8727555510959));
#35534=CARTESIAN_POINT('Ctrl Pts',(-21.7900839706634,26.2517168588919,-11.8666059022515));
#35535=CARTESIAN_POINT('Ctrl Pts',(-21.8747451782836,26.305025930145,-11.8604562534072));
#35536=CARTESIAN_POINT('Ctrl Pts',(-21.961681939521,26.354278393947,-11.8543066045629));
#35537=CARTESIAN_POINT('Ctrl Pts',(-21.9990573084783,26.375452739304,-11.8516627817284));
#35538=CARTESIAN_POINT('Ctrl Pts',(-22.0368529107137,26.3958778709974,-11.8490189588939));
#35539=CARTESIAN_POINT('Ctrl Pts',(-22.075036015346,26.4155367745563,-11.8463751360594));
#35540=CARTESIAN_POINT('Ctrl Pts',(-26.7730016580803,23.5526254787844,-12.6871150197353));
#35541=CARTESIAN_POINT('Ctrl Pts',(-26.7728024292441,23.823202332439,-12.704858087551));
#35542=CARTESIAN_POINT('Ctrl Pts',(-26.7385252597147,24.09268227854,-12.7235107134275));
#35543=CARTESIAN_POINT('Ctrl Pts',(-26.6524087047625,24.4267739169828,-12.746450801584));
#35544=CARTESIAN_POINT('Ctrl Pts',(-26.6313266338863,24.4982223453642,-12.7513366336673));
#35545=CARTESIAN_POINT('Ctrl Pts',(-26.5975699392434,24.5995470299869,-12.7581774061602));
#35546=CARTESIAN_POINT('Ctrl Pts',(-26.5868922639258,24.6300588393201,-12.7602255931275));
#35547=CARTESIAN_POINT('Ctrl Pts',(-26.5741762559277,24.6647138032508,-12.7625342434736));
#35548=CARTESIAN_POINT('Ctrl Pts',(-26.5725864670231,24.6690180119281,-12.762820668572));
#35549=CARTESIAN_POINT('Ctrl Pts',(-26.5701751351274,24.6755038217674,-12.7632517801217));
#35550=CARTESIAN_POINT('Ctrl Pts',(-26.5693604172905,24.6776879275158,-12.7633968737986));
#35551=CARTESIAN_POINT('Ctrl Pts',(-26.5678947764696,24.6816040546985,-12.7636568756696));
#35552=CARTESIAN_POINT('Ctrl Pts',(-26.5672447330568,24.6833363957719,-12.763771836472));
#35553=CARTESIAN_POINT('Ctrl Pts',(-26.5658407572021,24.687068164387,-12.7640193659137));
#35554=CARTESIAN_POINT('Ctrl Pts',(-26.5650863300132,24.689067396865,-12.7641519038925));
#35555=CARTESIAN_POINT('Ctrl Pts',(-26.563058028894,24.6944262546565,-12.7645069775629));
#35556=CARTESIAN_POINT('Ctrl Pts',(-26.5617805192994,24.6977845148843,-12.7647292941284));
#35557=CARTESIAN_POINT('Ctrl Pts',(-26.5559648426152,24.7129959073165,-12.7657354144316));
#35558=CARTESIAN_POINT('Ctrl Pts',(-26.5513622130052,24.7248245162577,-12.7665153847189));
#35559=CARTESIAN_POINT('Ctrl Pts',(-26.5457923528426,24.7388923782542,-12.7674404885065));
#35560=CARTESIAN_POINT('Ctrl Pts',(-26.5448923985021,24.7411578902946,-12.7675893905717));
#35561=CARTESIAN_POINT('Ctrl Pts',(-26.4172435973322,25.0614366671033,-12.7886291254906));
#35562=CARTESIAN_POINT('Ctrl Pts',(-26.240613571568,25.3572862510724,-12.8067442158744));
#35563=CARTESIAN_POINT('Ctrl Pts',(-25.9815636904075,25.6665118819232,-12.8297424468919));
#35564=CARTESIAN_POINT('Ctrl Pts',(-25.9411346004929,25.7120827699075,-12.8332477659115));
#35565=CARTESIAN_POINT('Ctrl Pts',(-25.8545985970419,25.8042262006905,-12.8406175107926));
#35566=CARTESIAN_POINT('Ctrl Pts',(-25.8083144823472,25.8505923875056,-12.8444873627208));
#35567=CARTESIAN_POINT('Ctrl Pts',(-25.735542368011,25.9191798118072,-12.8504898584851));
#35568=CARTESIAN_POINT('Ctrl Pts',(-25.7100550290956,25.9424400572493,-12.8525775674002));
#35569=CARTESIAN_POINT('Ctrl Pts',(-25.6788544142718,25.9700092284564,-12.8551179743324));
#35570=CARTESIAN_POINT('Ctrl Pts',(-25.673493320229,25.974714739824,-12.8555539484492));
#35571=CARTESIAN_POINT('Ctrl Pts',(-25.6656520438504,25.9815511884352,-12.8561908556173));
#35572=CARTESIAN_POINT('Ctrl Pts',(-25.6631841442848,25.9836962344931,-12.8563912014066));
#35573=CARTESIAN_POINT('Ctrl Pts',(-25.658265413252,25.9879583675865,-12.8567902926236));
#35574=CARTESIAN_POINT('Ctrl Pts',(-25.6558146464417,25.9900755236288,-12.8569890348515));
#35575=CARTESIAN_POINT('Ctrl Pts',(-25.6509200641132,25.9942909634285,-12.8573857471995));
#35576=CARTESIAN_POINT('Ctrl Pts',(-25.6484762856836,25.9963892849485,-12.857583715443));
#35577=CARTESIAN_POINT('Ctrl Pts',(-25.6425843515558,26.0014329989903,-12.8580607698772));
#35578=CARTESIAN_POINT('Ctrl Pts',(-25.6391331234176,26.0043747782121,-12.8583400047343));
#35579=CARTESIAN_POINT('Ctrl Pts',(-25.6285185519188,26.0133838797383,-12.8591982067779));
#35580=CARTESIAN_POINT('Ctrl Pts',(-25.6213349462069,26.0194271544861,-12.859778160131));
#35581=CARTESIAN_POINT('Ctrl Pts',(-25.536977335455,26.0897666491354,-12.8665789456912));
#35582=CARTESIAN_POINT('Ctrl Pts',(-25.456872187522,26.1504458433308,-12.8729455178736));
#35583=CARTESIAN_POINT('Ctrl Pts',(-25.2979634669048,26.2595228534622,-12.885425623497));
#35584=CARTESIAN_POINT('Ctrl Pts',(-25.2196515452597,26.308466414566,-12.8915118621672));
#35585=CARTESIAN_POINT('Ctrl Pts',(-25.0845001851517,26.3850676908425,-12.9018831248896));
#35586=CARTESIAN_POINT('Ctrl Pts',(-25.0287491052723,26.4145395819322,-12.9061250645356));
#35587=CARTESIAN_POINT('Ctrl Pts',(-24.8662734538015,26.4944216102783,-12.9183524596235));
#35588=CARTESIAN_POINT('Ctrl Pts',(-24.7575956753323,26.5406313776276,-12.9263720331903));
#35589=CARTESIAN_POINT('Ctrl Pts',(-24.5623748321191,26.6112578653706,-12.9403004435979));
#35590=CARTESIAN_POINT('Ctrl Pts',(-24.4768805779146,26.6382143416627,-12.9462456511234));
#35591=CARTESIAN_POINT('Ctrl Pts',(-24.3449861284423,26.6738283268949,-12.9550807304739));
#35592=CARTESIAN_POINT('Ctrl Pts',(-24.2993384833941,26.6850887412567,-12.9580781883776));
#35593=CARTESIAN_POINT('Ctrl Pts',(-24.2486074931249,26.6964315814224,-12.9613309029506));
#35594=CARTESIAN_POINT('Ctrl Pts',(-24.2437545419645,26.6975048615279,-12.96164126881));
#35595=CARTESIAN_POINT('Ctrl Pts',(-24.2365463402488,26.6990815475519,-12.9621010696985));
#35596=CARTESIAN_POINT('Ctrl Pts',(-24.2341930063927,26.6995935405289,-12.9622509969513));
#35597=CARTESIAN_POINT('Ctrl Pts',(-24.2301768826751,26.7004625773501,-12.9625065337299));
#35598=CARTESIAN_POINT('Ctrl Pts',(-24.2285143841615,26.7008209430052,-12.9626122199212));
#35599=CARTESIAN_POINT('Ctrl Pts',(-24.2251006174136,26.7015539820446,-12.9628290401184));
#35600=CARTESIAN_POINT('Ctrl Pts',(-24.2233493243553,26.7019285108406,-12.9629401655331));
#35601=CARTESIAN_POINT('Ctrl Pts',(-24.2191344626538,26.7028262212049,-12.9632073612932));
#35602=CARTESIAN_POINT('Ctrl Pts',(-24.2166705864744,26.7033479761302,-12.9633633490377));
#35603=CARTESIAN_POINT('Ctrl Pts',(-24.2076852516814,26.7052397245907,-12.9639314652179));
#35604=CARTESIAN_POINT('Ctrl Pts',(-24.2011601008287,26.706592390931,-12.9643426021408));
#35605=CARTESIAN_POINT('Ctrl Pts',(-24.0889762482193,26.7294854660483,-12.9713872796732));
#35606=CARTESIAN_POINT('Ctrl Pts',(-23.9822928871635,26.7457324794956,-12.9777245859901));
#35607=CARTESIAN_POINT('Ctrl Pts',(-23.6925062602712,26.7750813566795,-12.9944503465642));
#35608=CARTESIAN_POINT('Ctrl Pts',(-23.5087760349682,26.7779519890575,-13.0045503956241));
#35609=CARTESIAN_POINT('Ctrl Pts',(-23.2297184306843,26.7584686244722,-13.0202613815187));
#35610=CARTESIAN_POINT('Ctrl Pts',(-23.1339985601556,26.7474581379977,-13.0257141649896));
#35611=CARTESIAN_POINT('Ctrl Pts',(-22.9584398214559,26.7192459849636,-13.0359773131177));
#35612=CARTESIAN_POINT('Ctrl Pts',(-22.8784852439815,26.7032652081371,-13.0407535763453));
#35613=CARTESIAN_POINT('Ctrl Pts',(-22.7717218795319,26.6776807952038,-13.0473148002795));
#35614=CARTESIAN_POINT('Ctrl Pts',(-22.7443057286715,26.6707280072929,-13.0490161108776));
#35615=CARTESIAN_POINT('Ctrl Pts',(-22.7052863497455,26.6602841045353,-13.0514624536307));
#35616=CARTESIAN_POINT('Ctrl Pts',(-22.6936052887585,26.657086889631,-13.0521980221621));
#35617=CARTESIAN_POINT('Ctrl Pts',(-22.6730451426903,26.6513346205017,-13.053498517771));
#35618=CARTESIAN_POINT('Ctrl Pts',(-22.6641584564048,26.6488070675682,-13.0540625477542));
#35619=CARTESIAN_POINT('Ctrl Pts',(-22.6510779734098,26.6450258407694,-13.0548956258773));
#35620=CARTESIAN_POINT('Ctrl Pts',(-22.6468756100976,26.6438017648659,-13.055163706508));
#35621=CARTESIAN_POINT('Ctrl Pts',(-22.6396045970329,26.6416677652353,-13.0556283082512));
#35622=CARTESIAN_POINT('Ctrl Pts',(-22.6365347775454,26.6407618218769,-13.0558246988591));
#35623=CARTESIAN_POINT('Ctrl Pts',(-22.6304319193563,26.6389509018736,-13.0562155984939));
#35624=CARTESIAN_POINT('Ctrl Pts',(-22.6273988537835,26.6380460270364,-13.0564101040078));
#35625=CARTESIAN_POINT('Ctrl Pts',(-22.620225375751,26.6358944015734,-13.0568706786738));
#35626=CARTESIAN_POINT('Ctrl Pts',(-22.6160861369505,26.6346437855061,-13.0571368744195));
#35627=CARTESIAN_POINT('Ctrl Pts',(-22.6037756554997,26.630897283059,-13.0579298679471));
#35628=CARTESIAN_POINT('Ctrl Pts',(-22.5956118563361,26.6283772432643,-13.0584574583748));
#35629=CARTESIAN_POINT('Ctrl Pts',(-22.5203084058696,26.6048038311013,-13.0633399615579));
#35630=CARTESIAN_POINT('Ctrl Pts',(-22.4538697177707,26.5815908513199,-13.0677657831591));
#35631=CARTESIAN_POINT('Ctrl Pts',(-22.2813592805787,26.5149042724407,-13.0795851129866));
#35632=CARTESIAN_POINT('Ctrl Pts',(-22.176809626988,26.4679358190944,-13.0870856988103));
#35633=CARTESIAN_POINT('Ctrl Pts',(-22.0750356748951,26.4155365992721,-13.0947094732148));
#35634=CARTESIAN_POINT('',(-26.7730023334763,23.5513828472991,-12.9357734492733));
#35635=CARTESIAN_POINT('Ctrl Pts',(-22.0750360153462,26.4155367745563,-13.3428506325468));
#35636=CARTESIAN_POINT('Ctrl Pts',(-22.1633950675454,26.4610292011796,-13.3366796336625));
#35637=CARTESIAN_POINT('Ctrl Pts',(-22.254012492317,26.5025088954541,-13.3305086347781));
#35638=CARTESIAN_POINT('Ctrl Pts',(-22.3464881231975,26.5397456009848,-13.3243376358938));
#35639=CARTESIAN_POINT('Ctrl Pts',(-22.4388417141158,26.5769331652867,-13.3181747808682));
#35640=CARTESIAN_POINT('Ctrl Pts',(-22.5330482372733,26.6098887097839,-13.3120119258426));
#35641=CARTESIAN_POINT('Ctrl Pts',(-22.6286833006791,26.6384279986886,-13.305849070817));
#35642=CARTESIAN_POINT('Ctrl Pts',(-22.7242204126601,26.6669380570589,-13.2996925279159));
#35643=CARTESIAN_POINT('Ctrl Pts',(-22.8211827418363,26.6910407291222,-13.2935359850148));
#35644=CARTESIAN_POINT('Ctrl Pts',(-22.9191272056496,26.7106003583305,-13.2873794421138));
#35645=CARTESIAN_POINT('Ctrl Pts',(-23.01700470997,26.7301466156463,-13.2812271081182));
#35646=CARTESIAN_POINT('Ctrl Pts',(-23.1158625892922,26.7451559197203,-13.2750747741226));
#35647=CARTESIAN_POINT('Ctrl Pts',(-23.2152448092349,26.755543062737,-13.268922440127));
#35648=CARTESIAN_POINT('Ctrl Pts',(-23.3145925100241,26.7659265979113,-13.2627722430666));
#35649=CARTESIAN_POINT('Ctrl Pts',(-23.4144637578971,26.7716911170298,-13.2566220460062));
#35650=CARTESIAN_POINT('Ctrl Pts',(-23.5143954910274,26.7728030487745,-13.2504718489458));
#35651=CARTESIAN_POINT('Ctrl Pts',(-23.6143192487935,26.773914891778,-13.244322142721));
#35652=CARTESIAN_POINT('Ctrl Pts',(-23.7143030478139,26.7703748809936,-13.2381724364963));
#35653=CARTESIAN_POINT('Ctrl Pts',(-23.8138829186434,26.7622015632912,-13.2320227302716));
#35654=CARTESIAN_POINT('Ctrl Pts',(-23.9134814825028,26.7540267113021,-13.2258718696304));
#35655=CARTESIAN_POINT('Ctrl Pts',(-24.0126755345869,26.7412168602083,-13.2197210089892));
#35656=CARTESIAN_POINT('Ctrl Pts',(-24.1110063311914,26.7238424136496,-13.213570148348));
#35657=CARTESIAN_POINT('Ctrl Pts',(-24.2094440354683,26.706449077163,-13.2074126003391));
#35658=CARTESIAN_POINT('Ctrl Pts',(-24.307016181848,26.6844813124313,-13.2012550523302));
#35659=CARTESIAN_POINT('Ctrl Pts',(-24.4032744644503,26.6580606249871,-13.1950975043213));
#35660=CARTESIAN_POINT('Ctrl Pts',(-24.4995891995657,26.6316244426249,-13.1889363451005));
#35661=CARTESIAN_POINT('Ctrl Pts',(-24.5945881236382,26.6007302717376,-13.1827751858796));
#35662=CARTESIAN_POINT('Ctrl Pts',(-24.6878403224892,26.5655487991834,-13.1766140266588));
#35663=CARTESIAN_POINT('Ctrl Pts',(-24.781245215733,26.5303097192627,-13.1704427789416));
#35664=CARTESIAN_POINT('Ctrl Pts',(-24.8728972732914,26.4907694902959,-13.1642715312244));
#35665=CARTESIAN_POINT('Ctrl Pts',(-24.9623876519566,26.4471460341588,-13.1581002835073));
#35666=CARTESIAN_POINT('Ctrl Pts',(-25.0200526659792,26.4190363396041,-13.1541237098079));
#35667=CARTESIAN_POINT('Ctrl Pts',(-25.0768206287237,26.3892321664748,-13.1501471361085));
#35668=CARTESIAN_POINT('Ctrl Pts',(-25.1325885561893,26.3578013323538,-13.1461705624091));
#35669=CARTESIAN_POINT('Ctrl Pts',(-25.2191466754743,26.3090171294487,-13.1399984710968));
#35670=CARTESIAN_POINT('Ctrl Pts',(-25.3035990662544,26.2561403120594,-13.1338263797844));
#35671=CARTESIAN_POINT('Ctrl Pts',(-25.3855330115357,26.1993775047396,-13.1276542884721));
#35672=CARTESIAN_POINT('Ctrl Pts',(-25.4673559444213,26.142691605412,-13.1214905597333));
#35673=CARTESIAN_POINT('Ctrl Pts',(-25.5466668600733,26.0821304263655,-13.1153268309945));
#35674=CARTESIAN_POINT('Ctrl Pts',(-25.6230780267043,26.0179461977995,-13.1091631022557));
#35675=CARTESIAN_POINT('Ctrl Pts',(-25.6994082428757,25.9538299663998,-13.1030059034091));
#35676=CARTESIAN_POINT('Ctrl Pts',(-25.7728444866747,25.8860985941896,-13.0968487045624));
#35677=CARTESIAN_POINT('Ctrl Pts',(-25.8430292020959,25.8150467170809,-13.0906915057157));
#35678=CARTESIAN_POINT('Ctrl Pts',(-25.9131626167464,25.7440467745856,-13.084538807408));
#35679=CARTESIAN_POINT('Ctrl Pts',(-25.9800489238839,25.6697314607662,-13.0783861091003));
#35680=CARTESIAN_POINT('Ctrl Pts',(-26.0433654836239,25.5924340543361,-13.0722334107926));
#35681=CARTESIAN_POINT('Ctrl Pts',(-26.1066580336345,25.5151659591926,-13.0660830455968));
#35682=CARTESIAN_POINT('Ctrl Pts',(-26.1663832509785,25.4349183540323,-13.0599326804011));
#35683=CARTESIAN_POINT('Ctrl Pts',(-26.2222576588591,25.3520588927954,-13.0537823152054));
#35684=CARTESIAN_POINT('Ctrl Pts',(-26.278125827133,25.2692086846398,-13.0476326368331));
#35685=CARTESIAN_POINT('Ctrl Pts',(-26.3301437980267,25.1837475604556,-13.0414829584609));
#35686=CARTESIAN_POINT('Ctrl Pts',(-26.3780710411866,25.0960727152447,-13.0353332800887));
#35687=CARTESIAN_POINT('Ctrl Pts',(-26.4260057540636,25.0083842054406,-13.0291826432562));
#35688=CARTESIAN_POINT('Ctrl Pts',(-26.4698482644615,24.9184816705158,-13.0230320064238));
#35689=CARTESIAN_POINT('Ctrl Pts',(-26.5094041600705,24.8267865902989,-13.0168813695913));
#35690=CARTESIAN_POINT('Ctrl Pts',(-26.5490023721785,24.7349934156082,-13.0107241528695));
#35691=CARTESIAN_POINT('Ctrl Pts',(-26.5843046397494,24.6414042659238,-13.0045669361477));
#35692=CARTESIAN_POINT('Ctrl Pts',(-26.615164914666,24.5464601642719,-12.9984097194259));
#35693=CARTESIAN_POINT('Ctrl Pts',(-26.6460424064036,24.4514630936946,-12.9922490676181));
#35694=CARTESIAN_POINT('Ctrl Pts',(-26.6724728553308,24.3551099846848,-12.9860884158103));
#35695=CARTESIAN_POINT('Ctrl Pts',(-26.6943608269484,24.2578545315599,-12.9799277640025));
#35696=CARTESIAN_POINT('Ctrl Pts',(-26.7162854249259,24.1604363354774,-12.9737568032334));
#35697=CARTESIAN_POINT('Ctrl Pts',(-26.7336522868242,24.0621132071905,-12.9675858424644));
#35698=CARTESIAN_POINT('Ctrl Pts',(-26.7464175512049,23.963346625765,-12.9614148816953));
#35699=CARTESIAN_POINT('Ctrl Pts',(-26.7561615171861,23.8879562397308,-12.9567044714749));
#35700=CARTESIAN_POINT('Ctrl Pts',(-26.7632254033539,23.8123076353871,-12.9519940612545));
#35701=CARTESIAN_POINT('Ctrl Pts',(-26.7676101446616,23.7366058326589,-12.9472836510341));
#35702=CARTESIAN_POINT('Ctrl Pts',(-26.7711816140072,23.6749450301463,-12.9434469171139));
#35703=CARTESIAN_POINT('Ctrl Pts',(-26.7729806591481,23.6131805757407,-12.9396101831936));
#35704=CARTESIAN_POINT('Ctrl Pts',(-26.7730023334763,23.5513828472991,-12.9357734492733));
#35705=CARTESIAN_POINT('Ctrl Pts',(-26.773002271887,23.551546590173,-12.9329876023809));
#35706=CARTESIAN_POINT('Ctrl Pts',(-26.7731524659094,23.1775003206321,-12.91081626142));
#35707=CARTESIAN_POINT('Ctrl Pts',(-26.7081903843668,22.8062196535971,-12.891201579423));
#35708=CARTESIAN_POINT('Ctrl Pts',(-26.5659400232813,22.4128476063482,-12.8667037715344));
#35709=CARTESIAN_POINT('Ctrl Pts',(-26.5500998401361,22.3717039023126,-12.8640980270859));
#35710=CARTESIAN_POINT('Ctrl Pts',(-26.5166506260304,22.2898698166229,-12.8588177209579));
#35711=CARTESIAN_POINT('Ctrl Pts',(-26.4990360226658,22.2491922455496,-12.8561434403133));
#35712=CARTESIAN_POINT('Ctrl Pts',(-26.4773907378184,22.2019059434223,-12.8529716293445));
#35713=CARTESIAN_POINT('Ctrl Pts',(-26.4741677571019,22.1949310374084,-12.8525021482509));
#35714=CARTESIAN_POINT('Ctrl Pts',(-26.4691988615638,22.184277984974,-12.851782573542));
#35715=CARTESIAN_POINT('Ctrl Pts',(-26.467470852937,22.1805914769398,-12.8515331006168));
#35716=CARTESIAN_POINT('Ctrl Pts',(-26.4643108894116,22.1738831655274,-12.8510782888982));
#35717=CARTESIAN_POINT('Ctrl Pts',(-26.4628812063443,22.1708602931425,-12.8508730292272));
#35718=CARTESIAN_POINT('Ctrl Pts',(-26.4600007483429,22.1647943970046,-12.8504605076865));
#35719=CARTESIAN_POINT('Ctrl Pts',(-26.4585498982928,22.1617514137377,-12.8502532433975));
#35720=CARTESIAN_POINT('Ctrl Pts',(-26.4544172432108,22.1531185618607,-12.8496643253296));
#35721=CARTESIAN_POINT('Ctrl Pts',(-26.4517240892132,22.1475341703223,-12.8492822763588));
#35722=CARTESIAN_POINT('Ctrl Pts',(-26.4402993689607,22.1240181097122,-12.8476688167637));
#35723=CARTESIAN_POINT('Ctrl Pts',(-26.4314177029296,22.1061602301769,-12.8464321672748));
#35724=CARTESIAN_POINT('Ctrl Pts',(-26.2679660733681,21.7850279528911,-12.8239833824949));
#35725=CARTESIAN_POINT('Ctrl Pts',(-26.0665012933793,21.5081078148008,-12.8008691448452));
#35726=CARTESIAN_POINT('Ctrl Pts',(-25.7627511569584,21.2052932954409,-12.7719682453309));
#35727=CARTESIAN_POINT('Ctrl Pts',(-25.697376919529,21.1452904159161,-12.7660378382998));
#35728=CARTESIAN_POINT('Ctrl Pts',(-25.5934001439874,21.0574807248441,-12.7571301395297));
#35729=CARTESIAN_POINT('Ctrl Pts',(-25.5565211568815,21.0277041815248,-12.7540650881623));
#35730=CARTESIAN_POINT('Ctrl Pts',(-25.5070417292952,20.989525757529,-12.7500895456775));
#35731=CARTESIAN_POINT('Ctrl Pts',(-25.4950217798436,20.9803851873211,-12.7491341250556));
#35732=CARTESIAN_POINT('Ctrl Pts',(-25.4777393646855,20.9674334765861,-12.7477756668102));
#35733=CARTESIAN_POINT('Ctrl Pts',(-25.4725291467834,20.9635534035425,-12.7473680891556));
#35734=CARTESIAN_POINT('Ctrl Pts',(-25.4633153777544,20.9567350804184,-12.74665083707));
#35735=CARTESIAN_POINT('Ctrl Pts',(-25.4593167215666,20.9537902957313,-12.7463407187368));
#35736=CARTESIAN_POINT('Ctrl Pts',(-25.4533748080266,20.9494355585704,-12.7458816272946));
#35737=CARTESIAN_POINT('Ctrl Pts',(-25.4514367802767,20.9480185338774,-12.7457321622825));
#35738=CARTESIAN_POINT('Ctrl Pts',(-25.4480420440691,20.9455422266401,-12.7454708332372));
#35739=CARTESIAN_POINT('Ctrl Pts',(-25.446586030523,20.9444819992374,-12.7453589028189));
#35740=CARTESIAN_POINT('Ctrl Pts',(-25.4436761484083,20.9423668369706,-12.7451355160898));
#35741=CARTESIAN_POINT('Ctrl Pts',(-25.4422222906469,20.941311899882,-12.7450240595706));
#35742=CARTESIAN_POINT('Ctrl Pts',(-25.4382960369615,20.9384679697673,-12.7447234750262));
#35743=CARTESIAN_POINT('Ctrl Pts',(-25.4358219727111,20.9366812663585,-12.7445345072585));
#35744=CARTESIAN_POINT('Ctrl Pts',(-25.4266980409565,20.9301119042582,-12.7438392326342));
#35745=CARTESIAN_POINT('Ctrl Pts',(-25.4200324113546,20.9253510360491,-12.7433344275144));
#35746=CARTESIAN_POINT('Ctrl Pts',(-25.298674564842,20.8393690802654,-12.734199084352));
#35747=CARTESIAN_POINT('Ctrl Pts',(-25.1787916177853,20.7656986447333,-12.7260680688597));
#35748=CARTESIAN_POINT('Ctrl Pts',(-24.9846302895578,20.6632275365289,-12.7136275151696));
#35749=CARTESIAN_POINT('Ctrl Pts',(-24.913462658014,20.6289494657348,-12.7092098757905));
#35750=CARTESIAN_POINT('Ctrl Pts',(-24.6831034968294,20.5282495849825,-12.6951594426078));
#35751=CARTESIAN_POINT('Ctrl Pts',(-24.5198177797213,20.4719751898048,-12.6855507018088));
#35752=CARTESIAN_POINT('Ctrl Pts',(-24.280927648137,20.4105483487553,-12.671278267432));
#35753=CARTESIAN_POINT('Ctrl Pts',(-24.2084179640144,20.3945520471503,-12.666921882954));
#35754=CARTESIAN_POINT('Ctrl Pts',(-24.09229813527,20.3731111426938,-12.6598674146807));
#35755=CARTESIAN_POINT('Ctrl Pts',(-24.0490156063595,20.3660295575784,-12.6572211036155));
#35756=CARTESIAN_POINT('Ctrl Pts',(-23.9980190585062,20.3587510986307,-12.6540792190819));
#35757=CARTESIAN_POINT('Ctrl Pts',(-23.9904307200801,20.3576956534772,-12.6536110862217));
#35758=CARTESIAN_POINT('Ctrl Pts',(-23.9788088422864,20.3561214152225,-12.6528931516362));
#35759=CARTESIAN_POINT('Ctrl Pts',(-23.9747779281215,20.3555831766421,-12.6526439661935));
#35760=CARTESIAN_POINT('Ctrl Pts',(-23.967430913548,20.354616297627,-12.6521894555724));
#35761=CARTESIAN_POINT('Ctrl Pts',(-23.9641151395371,20.354185185022,-12.6519842089776));
#35762=CARTESIAN_POINT('Ctrl Pts',(-23.9574521696298,20.3533294169721,-12.6515715236388));
#35763=CARTESIAN_POINT('Ctrl Pts',(-23.9541049660027,20.3529048562381,-12.6513640821726));
#35764=CARTESIAN_POINT('Ctrl Pts',(-23.9445911794907,20.3517133012875,-12.6507741103193));
#35765=CARTESIAN_POINT('Ctrl Pts',(-23.9384230612519,20.3509588882919,-12.6503911824465));
#35766=CARTESIAN_POINT('Ctrl Pts',(-23.9123335540016,20.3478444802989,-12.64876965767));
#35767=CARTESIAN_POINT('Ctrl Pts',(-23.8923928795088,20.3456527208835,-12.6475257568095));
#35768=CARTESIAN_POINT('Ctrl Pts',(-23.4875771918388,20.3049792172327,-12.6221772488443));
#35769=CARTESIAN_POINT('Ctrl Pts',(-23.0989539909326,20.3359284799628,-12.5955154780121));
#35770=CARTESIAN_POINT('Ctrl Pts',(-22.6585667973289,20.4525476658325,-12.5651690911467));
#35771=CARTESIAN_POINT('Ctrl Pts',(-22.5924433775991,20.4723503556785,-12.5606257468027));
#35772=CARTESIAN_POINT('Ctrl Pts',(-22.4997655078763,20.5033820702191,-12.5543222641361));
#35773=CARTESIAN_POINT('Ctrl Pts',(-22.4726504326853,20.5128660822901,-12.5524860455227));
#35774=CARTESIAN_POINT('Ctrl Pts',(-22.4358667874512,20.5262864680318,-12.5500094730623));
#35775=CARTESIAN_POINT('Ctrl Pts',(-22.4260860915399,20.529908815673,-12.5493523573817));
#35776=CARTESIAN_POINT('Ctrl Pts',(-22.4116949087097,20.535318279142,-12.5483877347386));
#35777=CARTESIAN_POINT('Ctrl Pts',(-22.407070791694,20.5370685814245,-12.5480781294716));
#35778=CARTESIAN_POINT('Ctrl Pts',(-22.3997572995012,20.5398561140447,-12.5475890234976));
#35779=CARTESIAN_POINT('Ctrl Pts',(-22.3970652799823,20.5408863138105,-12.5474091101355));
#35780=CARTESIAN_POINT('Ctrl Pts',(-22.3919741662415,20.5428424493237,-12.5470690950192));
#35781=CARTESIAN_POINT('Ctrl Pts',(-22.3895747934566,20.5437676467346,-12.5469089493266));
#35782=CARTESIAN_POINT('Ctrl Pts',(-22.3854284464584,20.5453721802796,-12.5466323763116));
#35783=CARTESIAN_POINT('Ctrl Pts',(-22.3836809552352,20.546050169514,-12.5465158672869));
#35784=CARTESIAN_POINT('Ctrl Pts',(-22.3802975146165,20.5473662694471,-12.5462903910306));
#35785=CARTESIAN_POINT('Ctrl Pts',(-22.3786614977482,20.5480041916677,-12.5461814125325));
#35786=CARTESIAN_POINT('Ctrl Pts',(-22.3748039385112,20.5495119799014,-12.5459245626718));
#35787=CARTESIAN_POINT('Ctrl Pts',(-22.3725828353681,20.550382977725,-12.5457767600933));
#35788=CARTESIAN_POINT('Ctrl Pts',(-22.3660113332181,20.5529683924391,-12.5453397113533));
#35789=CARTESIAN_POINT('Ctrl Pts',(-22.3616636720064,20.5546898214716,-12.5450508870859));
#35790=CARTESIAN_POINT('Ctrl Pts',(-22.3233114661414,20.5699717767936,-12.5425058044055));
#35791=CARTESIAN_POINT('Ctrl Pts',(-22.2895347842532,20.5841020304023,-12.5402833577977));
#35792=CARTESIAN_POINT('Ctrl Pts',(-22.1056225849042,20.6647499298748,-12.5282484804328));
#35793=CARTESIAN_POINT('Ctrl Pts',(-21.9604813831869,20.7420998110335,-12.5189882438998));
#35794=CARTESIAN_POINT('Ctrl Pts',(-21.6962944421301,20.9099707236333,-12.501463874872));
#35795=CARTESIAN_POINT('Ctrl Pts',(-21.5764101303173,20.9983525922383,-12.4932074765565));
#35796=CARTESIAN_POINT('Ctrl Pts',(-21.3872608185746,21.159126904729,-12.4790753960702));
#35797=CARTESIAN_POINT('Ctrl Pts',(-21.3144880751643,21.2270285346655,-12.4733271236601));
#35798=CARTESIAN_POINT('Ctrl Pts',(-21.2001398894239,21.3440782892917,-12.4636468780076));
#35799=CARTESIAN_POINT('Ctrl Pts',(-21.156687035876,21.3912996475806,-12.459797341398));
#35800=CARTESIAN_POINT('Ctrl Pts',(-21.1091636886812,21.4461437797272,-12.455373824558));
#35801=CARTESIAN_POINT('Ctrl Pts',(-21.1036777773866,21.4525251068235,-12.4548598414543));
#35802=CARTESIAN_POINT('Ctrl Pts',(-21.0954758963984,21.462141644899,-12.4540863104182));
#35803=CARTESIAN_POINT('Ctrl Pts',(-21.0927411611016,21.4653608635524,-12.4538275367802));
#35804=CARTESIAN_POINT('Ctrl Pts',(-21.0880491283552,21.4709061909218,-12.4533820731343));
#35805=CARTESIAN_POINT('Ctrl Pts',(-21.0860887739371,21.4732297154619,-12.4531955090403));
#35806=CARTESIAN_POINT('Ctrl Pts',(-21.082058712602,21.4780201115581,-12.4528110496928));
#35807=CARTESIAN_POINT('Ctrl Pts',(-21.0799894099033,21.4804873177966,-12.4526131381517));
#35808=CARTESIAN_POINT('Ctrl Pts',(-21.0750172621702,21.4864336312706,-12.4521363748397));
#35809=CARTESIAN_POINT('Ctrl Pts',(-21.0721180555479,21.4899157604236,-12.4518573748193));
#35810=CARTESIAN_POINT('Ctrl Pts',(-21.0632450375034,21.5006186346117,-12.4510003976597));
#35811=CARTESIAN_POINT('Ctrl Pts',(-21.0572954109348,21.5078592837357,-12.4504214382343));
#35812=CARTESIAN_POINT('Ctrl Pts',(-20.9883888397283,21.5924677264314,-12.4436651755835));
#35813=CARTESIAN_POINT('Ctrl Pts',(-20.9290311542365,21.6726844620707,-12.4373441884769));
#35814=CARTESIAN_POINT('Ctrl Pts',(-20.7114289983159,21.9972274410809,-12.4120510206018));
#35815=CARTESIAN_POINT('Ctrl Pts',(-20.5828654837701,22.2597602822964,-12.3920253210485));
#35816=CARTESIAN_POINT('Ctrl Pts',(-20.4774455073804,22.5776728234169,-12.3696540344095));
#35817=CARTESIAN_POINT('Ctrl Pts',(-20.4644505572474,22.619725393383,-12.3667341243952));
#35818=CARTESIAN_POINT('Ctrl Pts',(-20.4379367785655,22.7122000830338,-12.3604160639647));
#35819=CARTESIAN_POINT('Ctrl Pts',(-20.4247728127029,22.7627130311901,-12.3570306995681));
#35820=CARTESIAN_POINT('Ctrl Pts',(-20.4090704948337,22.8295827095398,-12.3526543522629));
#35821=CARTESIAN_POINT('Ctrl Pts',(-20.4054233885426,22.8456680668642,-12.3516095775238));
#35822=CARTESIAN_POINT('Ctrl Pts',(-20.4004186496425,22.8685545403423,-12.3501350102391));
#35823=CARTESIAN_POINT('Ctrl Pts',(-20.398959302462,22.8753328169068,-12.349699772953));
#35824=CARTESIAN_POINT('Ctrl Pts',(-20.3967612723538,22.8857046419039,-12.3490361158524));
#35825=CARTESIAN_POINT('Ctrl Pts',(-20.3960068424366,22.8892947776155,-12.3488068207167));
#35826=CARTESIAN_POINT('Ctrl Pts',(-20.394778583634,22.8951897391341,-12.3484310272796));
#35827=CARTESIAN_POINT('Ctrl Pts',(-20.3943011483796,22.8974937973047,-12.3482843246371));
#35828=CARTESIAN_POINT('Ctrl Pts',(-20.3933997912314,22.9018677680449,-12.3480061663405));
#35829=CARTESIAN_POINT('Ctrl Pts',(-20.3929753810188,22.9039375770589,-12.3478746827219));
#35830=CARTESIAN_POINT('Ctrl Pts',(-20.3921875875827,22.9077988659029,-12.3476296663321));
#35831=CARTESIAN_POINT('Ctrl Pts',(-20.3918236942632,22.909590231534,-12.3475161045552));
#35832=CARTESIAN_POINT('Ctrl Pts',(-20.391086467587,22.9132353282144,-12.3472852482819));
#35833=CARTESIAN_POINT('Ctrl Pts',(-20.3907132430304,22.9150890711815,-12.347167960409));
#35834=CARTESIAN_POINT('Ctrl Pts',(-20.3896492384126,22.9203979452554,-12.3468323925823));
#35835=CARTESIAN_POINT('Ctrl Pts',(-20.3889624901199,22.9238538959309,-12.3466143448951));
#35836=CARTESIAN_POINT('Ctrl Pts',(-20.3860187284844,22.9387960511729,-12.34567329019));
#35837=CARTESIAN_POINT('Ctrl Pts',(-20.3838186005794,22.9502935674653,-12.344953509534));
#35838=CARTESIAN_POINT('Ctrl Pts',(-20.3809245233384,22.965877046188,-12.3439834803662));
#35839=CARTESIAN_POINT('Ctrl Pts',(-20.3801757718782,22.9699525489977,-12.3437303040536));
#35840=CARTESIAN_POINT('Ctrl Pts',(-20.3191771648423,23.3056133137435,-12.32291990611));
#35841=CARTESIAN_POINT('Ctrl Pts',(-20.3112901341222,23.6446596198105,-12.3050503199702));
#35842=CARTESIAN_POINT('Ctrl Pts',(-20.371301421233,24.091926941817,-12.2793604265429));
#35843=CARTESIAN_POINT('Ctrl Pts',(-20.3924732825126,24.2041391710111,-12.2727518455337));
#35844=CARTESIAN_POINT('Ctrl Pts',(-20.4314928611286,24.363879587465,-12.2629595046616));
#35845=CARTESIAN_POINT('Ctrl Pts',(-20.4445794635597,24.4124852321162,-12.2599279774414));
#35846=CARTESIAN_POINT('Ctrl Pts',(-20.4610426728404,24.4683827596517,-12.2563747013305));
#35847=CARTESIAN_POINT('Ctrl Pts',(-20.4633151716134,24.4759946127755,-12.2558893870087));
#35848=CARTESIAN_POINT('Ctrl Pts',(-20.4668108286694,24.4875474979495,-12.2551505747585));
#35849=CARTESIAN_POINT('Ctrl Pts',(-20.4680134629966,24.4914947496503,-12.2548977503613));
#35850=CARTESIAN_POINT('Ctrl Pts',(-20.4701963319781,24.4986102531169,-12.254441278492));
#35851=CARTESIAN_POINT('Ctrl Pts',(-20.4711738840452,24.5017793272449,-12.2542377193995));
#35852=CARTESIAN_POINT('Ctrl Pts',(-20.4731432483963,24.508128891344,-12.2538293492048));
#35853=CARTESIAN_POINT('Ctrl Pts',(-20.4741351042261,24.5113093635359,-12.2536245368763));
#35854=CARTESIAN_POINT('Ctrl Pts',(-20.4769280706857,24.5202166342024,-12.2530502012729));
#35855=CARTESIAN_POINT('Ctrl Pts',(-20.4787402472114,24.5259399243963,-12.2526803139572));
#35856=CARTESIAN_POINT('Ctrl Pts',(-20.4861701234834,24.5491794233054,-12.2511748863607));
#35857=CARTESIAN_POINT('Ctrl Pts',(-20.4919216671991,24.5666521773952,-12.2500349375313));
#35858=CARTESIAN_POINT('Ctrl Pts',(-20.6253699068414,24.9606672616657,-12.2241419078027));
#35859=CARTESIAN_POINT('Ctrl Pts',(-20.8215061009952,25.3103538651415,-12.196656796137));
#35860=CARTESIAN_POINT('Ctrl Pts',(-21.1404242787078,25.6924266010298,-12.1636044055868));
#35861=CARTESIAN_POINT('Ctrl Pts',(-21.2082799011705,25.7664093044123,-12.1570648596029));
#35862=CARTESIAN_POINT('Ctrl Pts',(-21.2827313059631,25.840336807273,-12.1504861054253));
#35863=CARTESIAN_POINT('Ctrl Pts',(-21.2859850160769,25.8435538892838,-12.1501997305347));
#35864=CARTESIAN_POINT('Ctrl Pts',(-21.2911918080841,25.8486801831239,-12.1497432774549));
#35865=CARTESIAN_POINT('Ctrl Pts',(-21.2931404695809,25.8505938457188,-12.1495728538394));
#35866=CARTESIAN_POINT('Ctrl Pts',(-21.2968512376721,25.8542287117108,-12.1492490969219));
#35867=CARTESIAN_POINT('Ctrl Pts',(-21.298612888035,25.8559503751212,-12.1490957274979));
#35868=CARTESIAN_POINT('Ctrl Pts',(-21.3017047683997,25.8589651513782,-12.1488271306));
#35869=CARTESIAN_POINT('Ctrl Pts',(-21.3030341423073,25.8602591365716,-12.1487118339197));
#35870=CARTESIAN_POINT('Ctrl Pts',(-21.3056447210455,25.8627958339153,-12.1484857884603));
#35871=CARTESIAN_POINT('Ctrl Pts',(-21.3069258375463,25.8640386263096,-12.1483750331223));
#35872=CARTESIAN_POINT('Ctrl Pts',(-21.3100009149295,25.8670167591795,-12.1481096016754));
#35873=CARTESIAN_POINT('Ctrl Pts',(-21.3117958639214,25.8687510843731,-12.1479550057664));
#35874=CARTESIAN_POINT('Ctrl Pts',(-21.3182900577626,25.8750113674683,-12.1473968864787));
#35875=CARTESIAN_POINT('Ctrl Pts',(-21.3230010704576,25.8795251777659,-12.1469943098849));
#35876=CARTESIAN_POINT('Ctrl Pts',(-21.3982043455782,25.9511436892873,-12.1406036309618));
#35877=CARTESIAN_POINT('Ctrl Pts',(-21.4716954094851,26.015043465493,-12.1348566866873));
#35878=CARTESIAN_POINT('Ctrl Pts',(-21.686833803462,26.1856258142931,-12.1190115702637));
#35879=CARTESIAN_POINT('Ctrl Pts',(-21.8345459780461,26.2840924171514,-12.1092270156187));
#35880=CARTESIAN_POINT('Ctrl Pts',(-22.0178611211012,26.3855543776125,-12.0974891941272));
#35881=CARTESIAN_POINT('Ctrl Pts',(-22.046338854748,26.4007617920497,-12.0956770989418));
#35882=CARTESIAN_POINT('Ctrl Pts',(-22.0750360352296,26.4155367847935,-12.0938589134715));
#35883=CARTESIAN_POINT('Origin',(-23.5502525316942,23.5502525316942,-77.3107734492734));
#35884=CARTESIAN_POINT('',(-22.075035905646,26.4155367180762,-10.5984952470527));
#35885=CARTESIAN_POINT('',(-22.0750360250409,26.4155367795477,-10.8457129588805));
#35886=CARTESIAN_POINT('',(-22.0750360153461,26.4155367745563,-77.3107734492734));
#35887=CARTESIAN_POINT('',(-26.7730017274927,23.5479758059353,-11.439226550727));
#35888=CARTESIAN_POINT('Ctrl Pts',(-22.075035905646,26.4155367180762,-10.5984952470527));
#35889=CARTESIAN_POINT('Ctrl Pts',(-22.0082494477041,26.3811511260226,-10.6027955967541));
#35890=CARTESIAN_POINT('Ctrl Pts',(-21.9426497206584,26.3444224858523,-10.6070294630284));
#35891=CARTESIAN_POINT('Ctrl Pts',(-21.6913677781022,26.191938982473,-10.6235035177627));
#35892=CARTESIAN_POINT('Ctrl Pts',(-21.5164249175405,26.0597343351953,-10.6355824193442));
#35893=CARTESIAN_POINT('Ctrl Pts',(-21.2836165715118,25.8433518425092,-10.6540810912497));
#35894=CARTESIAN_POINT('Ctrl Pts',(-21.2141697239007,25.7725614858273,-10.6599655885503));
#35895=CARTESIAN_POINT('Ctrl Pts',(-21.1418621279038,25.6917148288458,-10.6665675258275));
#35896=CARTESIAN_POINT('Ctrl Pts',(-21.1356550781298,25.6847136443714,-10.6671382957971));
#35897=CARTESIAN_POINT('Ctrl Pts',(-21.1264900636983,25.6742849131555,-10.6679871400436));
#35898=CARTESIAN_POINT('Ctrl Pts',(-21.1235086531116,25.6708779597656,-10.6682642351291));
#35899=CARTESIAN_POINT('Ctrl Pts',(-21.1184197109837,25.6650378769279,-10.6687388633998));
#35900=CARTESIAN_POINT('Ctrl Pts',(-21.1163086216336,25.6626078443408,-10.6689362483453));
#35901=CARTESIAN_POINT('Ctrl Pts',(-21.1120818100213,25.6577276973459,-10.6693324397305));
#35902=CARTESIAN_POINT('Ctrl Pts',(-21.1099661320312,25.6552775503964,-10.6695312476259));
#35903=CARTESIAN_POINT('Ctrl Pts',(-21.1050864217937,25.6496091604009,-10.6699909464535));
#35904=CARTESIAN_POINT('Ctrl Pts',(-21.1023250499135,25.6463886444428,-10.6702519469213));
#35905=CARTESIAN_POINT('Ctrl Pts',(-21.093997466427,25.6366375030656,-10.671041675918));
#35906=CARTESIAN_POINT('Ctrl Pts',(-21.0884510043524,25.6300901292264,-10.6715712164442));
#35907=CARTESIAN_POINT('Ctrl Pts',(-21.0758206225907,25.6150591672939,-10.6727852929513));
#35908=CARTESIAN_POINT('Ctrl Pts',(-21.0687540928762,25.6065611681707,-10.6734705331395));
#35909=CARTESIAN_POINT('Ctrl Pts',(-21.0048399583152,25.5288906698619,-10.6797233476217));
#35910=CARTESIAN_POINT('Ctrl Pts',(-20.9508593489849,25.4574196888613,-10.6854056464397));
#35911=CARTESIAN_POINT('Ctrl Pts',(-20.7880815475201,25.2221303907948,-10.7039121548336));
#35912=CARTESIAN_POINT('Ctrl Pts',(-20.6912760989912,25.0505856021648,-10.7171419390181));
#35913=CARTESIAN_POINT('Ctrl Pts',(-20.5261971030751,24.6832631794334,-10.7444021448771));
#35914=CARTESIAN_POINT('Ctrl Pts',(-20.4599138771022,24.4875100927262,-10.7583729946229));
#35915=CARTESIAN_POINT('Ctrl Pts',(-20.4099679292265,24.2747401200836,-10.77215675483));
#35916=CARTESIAN_POINT('Ctrl Pts',(-20.4072184980087,24.2627177764797,-10.7729308746654));
#35917=CARTESIAN_POINT('Ctrl Pts',(-20.4037566469526,24.2471701291711,-10.7739256408794));
#35918=CARTESIAN_POINT('Ctrl Pts',(-20.4029810687037,24.2436592153334,-10.7741498581627));
#35919=CARTESIAN_POINT('Ctrl Pts',(-20.4018034797623,24.2382857869489,-10.7744923751738));
#35920=CARTESIAN_POINT('Ctrl Pts',(-20.4013972457082,24.2364242164129,-10.7746109182515));
#35921=CARTESIAN_POINT('Ctrl Pts',(-20.4006365236844,24.23292329984,-10.7748336291285));
#35922=CARTESIAN_POINT('Ctrl Pts',(-20.4002816659728,24.2312840439842,-10.7749378178886));
#35923=CARTESIAN_POINT('Ctrl Pts',(-20.3994672185931,24.2275074707945,-10.7751776385289));
#35924=CARTESIAN_POINT('Ctrl Pts',(-20.3990085247228,24.2253699662078,-10.7753132179515));
#35925=CARTESIAN_POINT('Ctrl Pts',(-20.3977357692289,24.2194093917535,-10.7756908574139));
#35926=CARTESIAN_POINT('Ctrl Pts',(-20.3969264838941,24.2155852887705,-10.7759326419409));
#35927=CARTESIAN_POINT('Ctrl Pts',(-20.3924181847837,24.1940892946679,-10.7772890190434));
#35928=CARTESIAN_POINT('Ctrl Pts',(-20.3888606733955,24.1763875760883,-10.7783955862215));
#35929=CARTESIAN_POINT('Ctrl Pts',(-20.3789811070337,24.1249959633797,-10.7815805502338));
#35930=CARTESIAN_POINT('Ctrl Pts',(-20.3730473285589,24.0912329082794,-10.7836387121224));
#35931=CARTESIAN_POINT('Ctrl Pts',(-20.3521057749331,23.9598092258375,-10.7915398835067));
#35932=CARTESIAN_POINT('Ctrl Pts',(-20.3410523111349,23.8615666652851,-10.7972116468456));
#35933=CARTESIAN_POINT('Ctrl Pts',(-20.3140457034024,23.4532874682306,-10.8203683713949));
#35934=CARTESIAN_POINT('Ctrl Pts',(-20.3383976973719,23.1423005812777,-10.8372038792582));
#35935=CARTESIAN_POINT('Ctrl Pts',(-20.4186737860706,22.7872228011523,-10.8588362377704));
#35936=CARTESIAN_POINT('Ctrl Pts',(-20.4318185359028,22.7351643759521,-10.8620650350633));
#35937=CARTESIAN_POINT('Ctrl Pts',(-20.4486157215334,22.6750133737784,-10.8658708168336));
#35938=CARTESIAN_POINT('Ctrl Pts',(-20.4510091165323,22.6665757033945,-10.866406400639));
#35939=CARTESIAN_POINT('Ctrl Pts',(-20.4546260174877,22.6540201399369,-10.8672059823003));
#35940=CARTESIAN_POINT('Ctrl Pts',(-20.4558233762952,22.6498947042575,-10.8674691255744));
#35941=CARTESIAN_POINT('Ctrl Pts',(-20.4579729436409,22.6425434237791,-10.8679387874319));
#35942=CARTESIAN_POINT('Ctrl Pts',(-20.4589219624818,22.6393166464641,-10.8681452013827));
#35943=CARTESIAN_POINT('Ctrl Pts',(-20.4609113324972,22.6325914620952,-10.8685759504609));
#35944=CARTESIAN_POINT('Ctrl Pts',(-20.4619525782567,22.6290933265964,-10.8688003146477));
#35945=CARTESIAN_POINT('Ctrl Pts',(-20.4646906064705,22.6199515600604,-10.8693874611124));
#35946=CARTESIAN_POINT('Ctrl Pts',(-20.466396924869,22.6143108199795,-10.8697505557558));
#35947=CARTESIAN_POINT('Ctrl Pts',(-20.4701575613993,22.6020008587639,-10.8705447275384));
#35948=CARTESIAN_POINT('Ctrl Pts',(-20.4722180853762,22.5953335784315,-10.8709760074188));
#35949=CARTESIAN_POINT('Ctrl Pts',(-20.4783066341009,22.575857199754,-10.8722392301557));
#35950=CARTESIAN_POINT('Ctrl Pts',(-20.4823930396295,22.5630666379553,-10.8730730919133));
#35951=CARTESIAN_POINT('Ctrl Pts',(-20.4966398415405,22.5194166406222,-10.8759336372528));
#35952=CARTESIAN_POINT('Ctrl Pts',(-20.5071866270585,22.4886862967091,-10.8779730079546));
#35953=CARTESIAN_POINT('Ctrl Pts',(-20.5556435566923,22.354156505536,-10.8870161497905));
#35954=CARTESIAN_POINT('Ctrl Pts',(-20.5984096548996,22.2521971694377,-10.8941782101637));
#35955=CARTESIAN_POINT('Ctrl Pts',(-20.7947489100216,21.8442464939157,-10.9240873062915));
#35956=CARTESIAN_POINT('Ctrl Pts',(-20.991331870595,21.56149464271,-10.9480900724662));
#35957=CARTESIAN_POINT('Ctrl Pts',(-21.230423468183,21.3131747745721,-10.9698780231028));
#35958=CARTESIAN_POINT('Ctrl Pts',(-21.2321543765422,21.3113812271125,-10.9700354201093));
#35959=CARTESIAN_POINT('Ctrl Pts',(-21.2426843049032,21.3004955379876,-10.9709908828255));
#35960=CARTESIAN_POINT('Ctrl Pts',(-21.2515348936091,21.2914530972571,-10.9717852526862));
#35961=CARTESIAN_POINT('Ctrl Pts',(-21.2629939245468,21.2798827793163,-10.9728023082248));
#35962=CARTESIAN_POINT('Ctrl Pts',(-21.2655535425654,21.2773070246778,-10.97302876204));
#35963=CARTESIAN_POINT('Ctrl Pts',(-21.2694679372964,21.2733812454079,-10.9733739590075));
#35964=CARTESIAN_POINT('Ctrl Pts',(-21.2708195603943,21.2720281025055,-10.9734929515035));
#35965=CARTESIAN_POINT('Ctrl Pts',(-21.2733585774839,21.2694907519356,-10.9737160971687));
#35966=CARTESIAN_POINT('Ctrl Pts',(-21.2745456867866,21.2683062722913,-10.973820272082));
#35967=CARTESIAN_POINT('Ctrl Pts',(-21.2772758249208,21.2655864311053,-10.9740594972554));
#35968=CARTESIAN_POINT('Ctrl Pts',(-21.2788194822835,21.2640517087508,-10.9741944961222));
#35969=CARTESIAN_POINT('Ctrl Pts',(-21.2831090223769,21.2597956304971,-10.9745689098273));
#35970=CARTESIAN_POINT('Ctrl Pts',(-21.2858582602591,21.2570776382453,-10.9748080567713));
#35971=CARTESIAN_POINT('Ctrl Pts',(-21.3010320960005,21.2421301509825,-10.9761235078629));
#35972=CARTESIAN_POINT('Ctrl Pts',(-21.3135511909019,21.2299963740798,-10.977192345543));
#35973=CARTESIAN_POINT('Ctrl Pts',(-21.5305602912756,21.0230551775137,-10.9954519356519));
#35974=CARTESIAN_POINT('Ctrl Pts',(-21.7597239494885,20.855823252836,-11.0107537959102));
#35975=CARTESIAN_POINT('Ctrl Pts',(-22.1614378749016,20.6368469007539,-11.0364672597661));
#35976=CARTESIAN_POINT('Ctrl Pts',(-22.3216283847113,20.5657575972518,-11.0464636290546));
#35977=CARTESIAN_POINT('Ctrl Pts',(-22.4930629474543,20.505829437058,-11.0573218973698));
#35978=CARTESIAN_POINT('Ctrl Pts',(-22.4993479860483,20.503654194018,-11.0577201606163));
#35979=CARTESIAN_POINT('Ctrl Pts',(-22.5126030217927,20.4991125418319,-11.0585605066676));
#35980=CARTESIAN_POINT('Ctrl Pts',(-22.5195744753416,20.4967505281018,-11.0590027261689));
#35981=CARTESIAN_POINT('Ctrl Pts',(-22.5540512732195,20.4852008890178,-11.0611909716551));
#35982=CARTESIAN_POINT('Ctrl Pts',(-22.5816709864127,20.47636115022,-11.0629480392461));
#35983=CARTESIAN_POINT('Ctrl Pts',(-22.6155540793369,20.4660188031581,-11.0651096750472));
#35984=CARTESIAN_POINT('Ctrl Pts',(-22.6217081720238,20.4641604623841,-11.0655025310838));
#35985=CARTESIAN_POINT('Ctrl Pts',(-22.6318678553787,20.4611257008009,-11.066151507628));
#35986=CARTESIAN_POINT('Ctrl Pts',(-22.6358702649024,20.4599386219186,-11.0664072787073));
#35987=CARTESIAN_POINT('Ctrl Pts',(-22.6430893657167,20.4578127535847,-11.0668688065347));
#35988=CARTESIAN_POINT('Ctrl Pts',(-22.6463052412599,20.4568711961777,-11.0670744723894));
#35989=CARTESIAN_POINT('Ctrl Pts',(-22.6525430464783,20.4550554234331,-11.0674735389025));
#35990=CARTESIAN_POINT('Ctrl Pts',(-22.655564800337,20.4541806135888,-11.0676669198558));
#35991=CARTESIAN_POINT('Ctrl Pts',(-22.6640051054853,20.4517504997816,-11.0682072458707));
#35992=CARTESIAN_POINT('Ctrl Pts',(-22.6694264446796,20.4502049923786,-11.0685545103682));
#35993=CARTESIAN_POINT('Ctrl Pts',(-22.6915668349342,20.4439560090704,-11.0699735717799));
#35994=CARTESIAN_POINT('Ctrl Pts',(-22.7083194801779,20.4393735674711,-11.0710493044085));
#35995=CARTESIAN_POINT('Ctrl Pts',(-22.7508666453998,20.4281042619805,-11.0737867515267));
#35996=CARTESIAN_POINT('Ctrl Pts',(-22.7767081808666,20.421601595307,-11.0754543662919));
#35997=CARTESIAN_POINT('Ctrl Pts',(-22.8807084565449,20.3967985822548,-11.0821871359502));
#35998=CARTESIAN_POINT('Ctrl Pts',(-22.9594525628269,20.38110206654,-11.0873340918957));
#35999=CARTESIAN_POINT('Ctrl Pts',(-23.1356781981863,20.3527700081307,-11.0989630364996));
#36000=CARTESIAN_POINT('Ctrl Pts',(-23.2333162799396,20.3416211684696,-11.1054806736465));
#36001=CARTESIAN_POINT('Ctrl Pts',(-23.6133184023116,20.3157447197496,-11.1310357498993));
#36002=CARTESIAN_POINT('Ctrl Pts',(-23.896637817994,20.333725045191,-11.1506051927682));
#36003=CARTESIAN_POINT('Ctrl Pts',(-24.1753540336778,20.3887073991743,-11.168570128039));
#36004=CARTESIAN_POINT('Ctrl Pts',(-24.1767239667431,20.3889785711165,-11.1686583936659));
#36005=CARTESIAN_POINT('Ctrl Pts',(-24.1919492603721,20.3920026333742,-11.1696389786119));
#36006=CARTESIAN_POINT('Ctrl Pts',(-24.2057868564855,20.3948457626159,-11.1705265982599));
#36007=CARTESIAN_POINT('Ctrl Pts',(-24.2232656457137,20.3985569704711,-11.1716428484581));
#36008=CARTESIAN_POINT('Ctrl Pts',(-24.2269243468718,20.399340470535,-11.1718762304354));
#36009=CARTESIAN_POINT('Ctrl Pts',(-24.2327042705662,20.4005887556591,-11.172244478921));
#36010=CARTESIAN_POINT('Ctrl Pts',(-24.2348263875254,20.4010493127931,-11.1723795881609));
#36011=CARTESIAN_POINT('Ctrl Pts',(-24.2387700793088,20.4019093758691,-11.1726304944831));
#36012=CARTESIAN_POINT('Ctrl Pts',(-24.2405917615,20.4023083155387,-11.1727463232345));
#36013=CARTESIAN_POINT('Ctrl Pts',(-24.2446529863457,20.4032013991681,-11.173004392791));
#36014=CARTESIAN_POINT('Ctrl Pts',(-24.2468923430636,20.4036963514476,-11.1731465859687));
#36015=CARTESIAN_POINT('Ctrl Pts',(-24.253433684206,20.4051494722824,-11.1735616383687));
#36016=CARTESIAN_POINT('Ctrl Pts',(-24.2577342556955,20.4061140808109,-11.1738341264483));
#36017=CARTESIAN_POINT('Ctrl Pts',(-24.2888364748846,20.4131572833891,-11.1758020859789));
#36018=CARTESIAN_POINT('Ctrl Pts',(-24.3155624307594,20.4195699035218,-11.1774785997989));
#36019=CARTESIAN_POINT('Ctrl Pts',(-24.3997830938571,20.4409208042443,-11.1827250822084));
#36020=CARTESIAN_POINT('Ctrl Pts',(-24.4569513897218,20.4571078386367,-11.186232066871));
#36021=CARTESIAN_POINT('Ctrl Pts',(-24.6541301853821,20.518875772836,-11.1982414241774));
#36022=CARTESIAN_POINT('Ctrl Pts',(-24.7914468020693,20.5724624331988,-11.2064564775664));
#36023=CARTESIAN_POINT('Ctrl Pts',(-24.9883225854023,20.6652861117598,-11.2186184015814));
#36024=CARTESIAN_POINT('Ctrl Pts',(-25.0510170334093,20.6973973936696,-11.2225514401361));
#36025=CARTESIAN_POINT('Ctrl Pts',(-25.1983638424373,20.7790686716482,-11.2320302319616));
#36026=CARTESIAN_POINT('Ctrl Pts',(-25.2819010856265,20.8304873975059,-11.2375993406465));
#36027=CARTESIAN_POINT('Ctrl Pts',(-25.38622187057,20.9014555161335,-11.2449142389547));
#36028=CARTESIAN_POINT('Ctrl Pts',(-25.4092742200644,20.9175832887211,-11.2465542440943));
#36029=CARTESIAN_POINT('Ctrl Pts',(-25.4455196241831,20.9436545606976,-11.2491729601276));
#36030=CARTESIAN_POINT('Ctrl Pts',(-25.4588527197663,20.9534014302927,-11.2501450625548));
#36031=CARTESIAN_POINT('Ctrl Pts',(-25.4843148395328,20.9723169792927,-11.2520189746015));
#36032=CARTESIAN_POINT('Ctrl Pts',(-25.4964550711007,20.9814698652471,-11.2529202116714));
#36033=CARTESIAN_POINT('Ctrl Pts',(-25.5139768055794,20.9948755392144,-11.2542325524569));
#36034=CARTESIAN_POINT('Ctrl Pts',(-25.5194103259272,20.9990602265348,-11.2546411475155));
#36035=CARTESIAN_POINT('Ctrl Pts',(-25.5348013812039,21.0109922849481,-11.2558032425856));
#36036=CARTESIAN_POINT('Ctrl Pts',(-25.5447267602058,21.0187807696688,-11.2565582743586));
#36037=CARTESIAN_POINT('Ctrl Pts',(-25.563879979986,21.0339929423079,-11.2580264099037));
#36038=CARTESIAN_POINT('Ctrl Pts',(-25.5731131451546,21.0414096201995,-11.2587392362961));
#36039=CARTESIAN_POINT('Ctrl Pts',(-25.5860466530475,21.0519164663021,-11.2597450291674));
#36040=CARTESIAN_POINT('Ctrl Pts',(-25.5897813378104,21.0549643622012,-11.2600363244526));
#36041=CARTESIAN_POINT('Ctrl Pts',(-25.6087842899706,21.0705439347006,-11.2615229300539));
#36042=CARTESIAN_POINT('Ctrl Pts',(-25.6239436950967,21.0832072022289,-11.262723465729));
#36043=CARTESIAN_POINT('Ctrl Pts',(-25.6436887753596,21.1000116455906,-11.2643068716919));
#36044=CARTESIAN_POINT('Ctrl Pts',(-25.6483805324044,21.1040279716789,-11.264684594379));
#36045=CARTESIAN_POINT('Ctrl Pts',(-25.6556116213914,21.1102541715505,-11.2652690564658));
#36046=CARTESIAN_POINT('Ctrl Pts',(-25.6581591023426,21.1124545943428,-11.2654754039147));
#36047=CARTESIAN_POINT('Ctrl Pts',(-25.6632304535699,21.1168489384932,-11.2658870751226));
#36048=CARTESIAN_POINT('Ctrl Pts',(-25.6657543659634,21.1190428050749,-11.2660923964613));
#36049=CARTESIAN_POINT('Ctrl Pts',(-25.6706893373576,21.1233459455328,-11.2664947246509));
#36050=CARTESIAN_POINT('Ctrl Pts',(-25.6731006756701,21.1254548943098,-11.2666917177957));
#36051=CARTESIAN_POINT('Ctrl Pts',(-25.6785040067931,21.1301948680034,-11.2671340559293));
#36052=CARTESIAN_POINT('Ctrl Pts',(-25.6814942691802,21.1328278497199,-11.2673794827075));
#36053=CARTESIAN_POINT('Ctrl Pts',(-25.6951326345143,21.1448816577241,-11.2685017565974));
#36054=CARTESIAN_POINT('Ctrl Pts',(-25.7057230773603,21.1543672228431,-11.2693813219542));
#36055=CARTESIAN_POINT('Ctrl Pts',(-25.7804233902968,21.2221703776673,-11.2756437333455));
#36056=CARTESIAN_POINT('Ctrl Pts',(-25.8422152319003,21.282978128385,-11.281132823447));
#36057=CARTESIAN_POINT('Ctrl Pts',(-25.9458151347108,21.3934956288553,-11.2909080674684));
#36058=CARTESIAN_POINT('Ctrl Pts',(-25.9887131343269,21.4421183906944,-11.2951464215273));
#36059=CARTESIAN_POINT('Ctrl Pts',(-26.2480944317104,21.7546307550851,-11.321984194109));
#36060=CARTESIAN_POINT('Ctrl Pts',(-26.4229508008435,22.0501891559384,-11.3459160403214));
#36061=CARTESIAN_POINT('Ctrl Pts',(-26.549192806043,22.370217626214,-11.3676612623035));
#36062=CARTESIAN_POINT('Ctrl Pts',(-26.5502001289748,22.3727808501055,-11.3678351596448));
#36063=CARTESIAN_POINT('Ctrl Pts',(-26.5557492502397,22.3869544334551,-11.3687952480426));
#36064=CARTESIAN_POINT('Ctrl Pts',(-26.5602270181877,22.3985899972243,-11.3695778836949));
#36065=CARTESIAN_POINT('Ctrl Pts',(-26.5659144525721,22.4136286808745,-11.3705820298454));
#36066=CARTESIAN_POINT('Ctrl Pts',(-26.5671859982344,22.4170080487784,-11.370807193563));
#36067=CARTESIAN_POINT('Ctrl Pts',(-26.5691209391378,22.4221768502446,-11.3711508447404));
#36068=CARTESIAN_POINT('Ctrl Pts',(-26.5697884232705,22.4239647336315,-11.371269578078));
#36069=CARTESIAN_POINT('Ctrl Pts',(-26.571039506128,22.427324915916,-11.3714924722904));
#36070=CARTESIAN_POINT('Ctrl Pts',(-26.571623463354,22.4288970713062,-11.3715966544587));
#36071=CARTESIAN_POINT('Ctrl Pts',(-26.5729644043445,22.4325158636334,-11.3718362195848));
#36072=CARTESIAN_POINT('Ctrl Pts',(-26.5737205354696,22.4345628103097,-11.3719715505402));
#36073=CARTESIAN_POINT('Ctrl Pts',(-26.5758189525608,22.4402613016097,-11.3723478084771));
#36074=CARTESIAN_POINT('Ctrl Pts',(-26.5771567120487,22.4439145267105,-11.372588463221));
#36075=CARTESIAN_POINT('Ctrl Pts',(-26.5845733955768,22.4642825531138,-11.3739271330178));
#36076=CARTESIAN_POINT('Ctrl Pts',(-26.5905206402388,22.4810454602382,-11.3750173671274));
#36077=CARTESIAN_POINT('Ctrl Pts',(-26.6844521437447,22.7529228893475,-11.3925276521857));
#36078=CARTESIAN_POINT('Ctrl Pts',(-26.7402056058759,23.0180934710657,-11.4072228653874));
#36079=CARTESIAN_POINT('Ctrl Pts',(-26.7693552008018,23.3739537078708,-11.427249448118));
#36080=CARTESIAN_POINT('Ctrl Pts',(-26.772943488292,23.4610070063838,-11.4321654148819));
#36081=CARTESIAN_POINT('Ctrl Pts',(-26.7730018090362,23.5480943167315,-11.4371602447912));
#36082=CARTESIAN_POINT('Ctrl Pts',(-22.075036015346,26.4155367745563,-11.8463751360594));
#36083=CARTESIAN_POINT('Ctrl Pts',(-22.1638791174928,26.4612784185055,-11.8402235822661));
#36084=CARTESIAN_POINT('Ctrl Pts',(-22.254821394332,26.5028685328931,-11.8340720284728));
#36085=CARTESIAN_POINT('Ctrl Pts',(-22.3474353189619,26.5401268292617,-11.8279204746795));
#36086=CARTESIAN_POINT('Ctrl Pts',(-22.440153973422,26.5774272581181,-11.8217619645761));
#36087=CARTESIAN_POINT('Ctrl Pts',(-22.5345476448762,26.6103859303396,-11.8156034544726));
#36088=CARTESIAN_POINT('Ctrl Pts',(-22.6301710703149,26.638871586697,-11.8094449443692));
#36089=CARTESIAN_POINT('Ctrl Pts',(-22.7258576981229,26.6673760706687,-11.8032823637942));
#36090=CARTESIAN_POINT('Ctrl Pts',(-22.8227752769979,26.6914015490826,-11.7971197832192));
#36091=CARTESIAN_POINT('Ctrl Pts',(-22.9204677005841,26.7108677612031,-11.7909572026442));
#36092=CARTESIAN_POINT('Ctrl Pts',(-23.0183113022632,26.730364097101,-11.7847850855346));
#36093=CARTESIAN_POINT('Ctrl Pts',(-23.1169317133489,26.7452870211307,-11.7786129684251));
#36094=CARTESIAN_POINT('Ctrl Pts',(-23.2158672180003,26.7556080540171,-11.7724408513155));
#36095=CARTESIAN_POINT('Ctrl Pts',(-23.2489383989166,26.7590580666999,-11.7703776971193));
#36096=CARTESIAN_POINT('Ctrl Pts',(-23.2820447872775,26.7619943119972,-11.7683145429232));
#36097=CARTESIAN_POINT('Ctrl Pts',(-23.3151691812701,26.7644170235728,-11.7662513887271));
#36098=CARTESIAN_POINT('Ctrl Pts',(-23.4142634635937,26.7716647596347,-11.7600792974147));
#36099=CARTESIAN_POINT('Ctrl Pts',(-23.5138677628276,26.7743382778831,-11.7539072061024));
#36100=CARTESIAN_POINT('Ctrl Pts',(-23.6135239629293,26.7723813758731,-11.7477351147901));
#36101=CARTESIAN_POINT('Ctrl Pts',(-23.7130451387318,26.7704271252718,-11.7415713860513));
#36102=CARTESIAN_POINT('Ctrl Pts',(-23.8126176451428,26.7638549326342,-11.7354076573125));
#36103=CARTESIAN_POINT('Ctrl Pts',(-23.9117789491918,26.752660408894,-11.7292439285737));
#36104=CARTESIAN_POINT('Ctrl Pts',(-24.010835201146,26.741477744701,-11.7230867297271));
#36105=CARTESIAN_POINT('Ctrl Pts',(-24.109480687534,26.7256825334003,-11.7169295308804));
#36106=CARTESIAN_POINT('Ctrl Pts',(-24.207254552655,26.7053224052395,-11.7107723320338));
#36107=CARTESIAN_POINT('Ctrl Pts',(-24.3049569510098,26.6849771590978,-11.7046196337261));
#36108=CARTESIAN_POINT('Ctrl Pts',(-24.4017885707688,26.6600737182635,-11.6984669354183));
#36109=CARTESIAN_POINT('Ctrl Pts',(-24.4972962640925,26.6307112201731,-11.6923142371106));
#36110=CARTESIAN_POINT('Ctrl Pts',(-24.5927677407629,26.6013598563838,-11.6861638719149));
#36111=CARTESIAN_POINT('Ctrl Pts',(-24.6869158737756,26.5675529226133,-11.6800135067191));
#36112=CARTESIAN_POINT('Ctrl Pts',(-24.7793011219447,26.5294398580138,-11.6738631415234));
#36113=CARTESIAN_POINT('Ctrl Pts',(-24.8716760532692,26.491331049576,-11.6677134631512));
#36114=CARTESIAN_POINT('Ctrl Pts',(-24.9622880895723,26.4489172320187,-11.6615637847789));
#36115=CARTESIAN_POINT('Ctrl Pts',(-25.0507171223673,26.4023962122679,-11.6554141064067));
#36116=CARTESIAN_POINT('Ctrl Pts',(-25.1391599372994,26.3558679419675,-11.6492634695743));
#36117=CARTESIAN_POINT('Ctrl Pts',(-25.2254186884504,26.3052314002832,-11.6431128327418));
#36118=CARTESIAN_POINT('Ctrl Pts',(-25.3090982499685,26.250730137935,-11.6369621959094));
#36119=CARTESIAN_POINT('Ctrl Pts',(-25.3928673310391,26.196170570685,-11.6308049791875));
#36120=CARTESIAN_POINT('Ctrl Pts',(-25.4740513479296,26.1377382642457,-11.6246477624657));
#36121=CARTESIAN_POINT('Ctrl Pts',(-25.5522846517356,26.0757198058481,-11.6184905457439));
#36122=CARTESIAN_POINT('Ctrl Pts',(-25.6305616015813,26.0136667476067,-11.6123298939361));
#36123=CARTESIAN_POINT('Ctrl Pts',(-25.7058842324766,25.9480238384593,-11.6061692421283));
#36124=CARTESIAN_POINT('Ctrl Pts',(-25.777922048037,25.8791162220928,-11.6000085903205));
#36125=CARTESIAN_POINT('Ctrl Pts',(-25.8500804084799,25.8100932987802,-11.5938376295515));
#36126=CARTESIAN_POINT('Ctrl Pts',(-25.9189426743867,25.7377950707075,-11.5876666687825));
#36127=CARTESIAN_POINT('Ctrl Pts',(-25.9842170045119,25.662581698174,-11.5814957080134));
#36128=CARTESIAN_POINT('Ctrl Pts',(-26.0340421262817,25.6051699187194,-11.576785297793));
#36129=CARTESIAN_POINT('Ctrl Pts',(-26.0817775161061,25.5460603392475,-11.5720748875726));
#36130=CARTESIAN_POINT('Ctrl Pts',(-26.1273105299634,25.4854242646566,-11.5673644773521));
#36131=CARTESIAN_POINT('Ctrl Pts',(-26.1872004936594,25.4056691156278,-11.5611688343846));
#36132=CARTESIAN_POINT('Ctrl Pts',(-26.2434912396094,25.3229891618407,-11.5549731914171));
#36133=CARTESIAN_POINT('Ctrl Pts',(-26.2958852886696,25.2377412950119,-11.5487775484496));
#36134=CARTESIAN_POINT('Ctrl Pts',(-26.348208064848,25.1526093929014,-11.5425903335638));
#36135=CARTESIAN_POINT('Ctrl Pts',(-26.3966444552897,25.0649168819929,-11.5364031186781));
#36136=CARTESIAN_POINT('Ctrl Pts',(-26.4409379947223,24.9750525584833,-11.5302159037923));
#36137=CARTESIAN_POINT('Ctrl Pts',(-26.4851828220737,24.8852870637933,-11.5240354933326));
#36138=CARTESIAN_POINT('Ctrl Pts',(-26.5252936662427,24.7933548872637,-11.5178550828729));
#36139=CARTESIAN_POINT('Ctrl Pts',(-26.5610585690881,24.6996717623026,-11.5116746724132));
#36140=CARTESIAN_POINT('Ctrl Pts',(-26.5967923198493,24.6060702375799,-11.5054996452385));
#36141=CARTESIAN_POINT('Ctrl Pts',(-26.6281875054638,24.5107211977596,-11.4993246180639));
#36142=CARTESIAN_POINT('Ctrl Pts',(-26.6550795643388,24.4140619203092,-11.4931495908892));
#36143=CARTESIAN_POINT('Ctrl Pts',(-26.6819573249434,24.3174540357435,-11.486977846922));
#36144=CARTESIAN_POINT('Ctrl Pts',(-26.7043366050413,24.2195377121399,-11.4808061029548));
#36145=CARTESIAN_POINT('Ctrl Pts',(-26.7221024170935,24.12076621864,-11.4746343589876));
#36146=CARTESIAN_POINT('Ctrl Pts',(-26.7398677128267,24.0219975956868,-11.4684627943867));
#36147=CARTESIAN_POINT('Ctrl Pts',(-26.7530197187827,23.922374272976,-11.4622912297859));
#36148=CARTESIAN_POINT('Ctrl Pts',(-26.7614945193228,23.8223599725909,-11.456119665185));
#36149=CARTESIAN_POINT('Ctrl Pts',(-26.7692270682408,23.7311052620432,-11.4504886270323));
#36150=CARTESIAN_POINT('Ctrl Pts',(-26.773066403134,23.6395254228175,-11.4448575888797));
#36151=CARTESIAN_POINT('Ctrl Pts',(-26.7730017274927,23.5479758059353,-11.439226550727));
#36152=CARTESIAN_POINT('Ctrl Pts',(-22.0750360352296,26.4155367847935,-12.0938589134715));
#36153=CARTESIAN_POINT('Ctrl Pts',(-22.141904313061,26.4499644987072,-12.0896222975693));
#36154=CARTESIAN_POINT('Ctrl Pts',(-22.2099640499397,26.4820443585534,-12.085352014354));
#36155=CARTESIAN_POINT('Ctrl Pts',(-22.3840259436386,26.5567576726363,-12.0744419892762));
#36156=CARTESIAN_POINT('Ctrl Pts',(-22.4912699591345,26.5961857486819,-12.0677275327897));
#36157=CARTESIAN_POINT('Ctrl Pts',(-22.6188477338851,26.6355363916311,-12.0596467714977));
#36158=CARTESIAN_POINT('Ctrl Pts',(-22.6373741276867,26.6410686679099,-12.0584711847134));
#36159=CARTESIAN_POINT('Ctrl Pts',(-22.6615979135229,26.6480654870124,-12.0569309472581));
#36160=CARTESIAN_POINT('Ctrl Pts',(-22.6672513804879,26.6496816892615,-12.0565712583184));
#36161=CARTESIAN_POINT('Ctrl Pts',(-22.6764445637053,26.6522826245131,-12.0559859934471));
#36162=CARTESIAN_POINT('Ctrl Pts',(-22.6799816141837,26.6532767970896,-12.0557607257635));
#36163=CARTESIAN_POINT('Ctrl Pts',(-22.6867726961014,26.6551730682862,-12.0553280420279));
#36164=CARTESIAN_POINT('Ctrl Pts',(-22.6900264621821,26.6560761059205,-12.0551206569004));
#36165=CARTESIAN_POINT('Ctrl Pts',(-22.697449662049,26.6581237520593,-12.0546473482485));
#36166=CARTESIAN_POINT('Ctrl Pts',(-22.7016199855978,26.6592650852654,-12.0543813185049));
#36167=CARTESIAN_POINT('Ctrl Pts',(-22.7146216392645,26.6627952660597,-12.05355152536));
#36168=CARTESIAN_POINT('Ctrl Pts',(-22.7234607952735,26.6651548870583,-12.0529868132175));
#36169=CARTESIAN_POINT('Ctrl Pts',(-22.7921855753088,26.6831878961381,-12.0485915007129));
#36170=CARTESIAN_POINT('Ctrl Pts',(-22.8524979207607,26.6971696184901,-12.0447064209677));
#36171=CARTESIAN_POINT('Ctrl Pts',(-22.9181075849285,26.7104005783717,-12.0404460099879));
#36172=CARTESIAN_POINT('Ctrl Pts',(-22.9230452281013,26.7113842765766,-12.0401251757339));
#36173=CARTESIAN_POINT('Ctrl Pts',(-22.9500891241205,26.7167062190314,-12.0383668140076));
#36174=CARTESIAN_POINT('Ctrl Pts',(-22.9722376679158,26.7208240649012,-12.0369226233702));
#36175=CARTESIAN_POINT('Ctrl Pts',(-23.2463070505,26.7688117159694,-12.0190010101658));
#36176=CARTESIAN_POINT('Ctrl Pts',(-23.5025106856627,26.782772831883,-12.0016087899334));
#36177=CARTESIAN_POINT('Ctrl Pts',(-23.8552716957069,26.76002778508,-11.9777539070983));
#36178=CARTESIAN_POINT('Ctrl Pts',(-23.9525965168783,26.7492860741959,-11.9711959680989));
#36179=CARTESIAN_POINT('Ctrl Pts',(-24.11077941454,26.7244928168055,-11.9607133646114));
#36180=CARTESIAN_POINT('Ctrl Pts',(-24.171984805859,26.7130743727495,-11.956701635958));
#36181=CARTESIAN_POINT('Ctrl Pts',(-24.2395641474985,26.6984289242487,-11.9523495509254));
#36182=CARTESIAN_POINT('Ctrl Pts',(-24.2462980068534,26.6969469561461,-11.951916755115));
#36183=CARTESIAN_POINT('Ctrl Pts',(-24.2565929360581,26.6946466140983,-11.9512564584681));
#36184=CARTESIAN_POINT('Ctrl Pts',(-24.2601574051069,26.6938437874575,-11.9510280928944));
#36185=CARTESIAN_POINT('Ctrl Pts',(-24.266009074252,26.6925153535603,-11.950653616417));
#36186=CARTESIAN_POINT('Ctrl Pts',(-24.2682970671439,26.6919933095259,-11.9505073031892));
#36187=CARTESIAN_POINT('Ctrl Pts',(-24.2727153673917,26.6909801214287,-11.9502249688609));
#36188=CARTESIAN_POINT('Ctrl Pts',(-24.274845748211,26.6904893082016,-11.9500889287986));
#36189=CARTESIAN_POINT('Ctrl Pts',(-24.2786848318684,26.6896007163373,-11.9498439467526));
#36190=CARTESIAN_POINT('Ctrl Pts',(-24.2803937023712,26.6892037118308,-11.9497349604602));
#36191=CARTESIAN_POINT('Ctrl Pts',(-24.2842271615044,26.6883098233958,-11.9494906120856));
#36192=CARTESIAN_POINT('Ctrl Pts',(-24.2863515654272,26.6878121782685,-11.9493552949786));
#36193=CARTESIAN_POINT('Ctrl Pts',(-24.2921608759784,26.6864451127616,-11.9489855164906));
#36194=CARTESIAN_POINT('Ctrl Pts',(-24.2958447733596,26.6855713522255,-11.948751306354));
#36195=CARTESIAN_POINT('Ctrl Pts',(-24.3137055949855,26.6813017964703,-11.9476170945413));
#36196=CARTESIAN_POINT('Ctrl Pts',(-24.3278612013306,26.677816256732,-11.9467222128187));
#36197=CARTESIAN_POINT('Ctrl Pts',(-24.3505279965161,26.6720715957018,-11.9452950480826));
#36198=CARTESIAN_POINT('Ctrl Pts',(-24.3590542171703,26.6698734903214,-11.9447595284686));
#36199=CARTESIAN_POINT('Ctrl Pts',(-24.3726481313066,26.6663094285981,-11.9439076586451));
#36200=CARTESIAN_POINT('Ctrl Pts',(-24.3777216102767,26.6649660067612,-11.943590159657));
#36201=CARTESIAN_POINT('Ctrl Pts',(-24.3871837336574,26.6624357515392,-11.9429987890098));
#36202=CARTESIAN_POINT('Ctrl Pts',(-24.3915731837441,26.6612520160465,-11.9427247638796));
#36203=CARTESIAN_POINT('Ctrl Pts',(-24.6979098770364,26.5779441716384,-11.9236214492977));
#36204=CARTESIAN_POINT('Ctrl Pts',(-24.9863370758769,26.4522797329199,-11.9069080461384));
#36205=CARTESIAN_POINT('Ctrl Pts',(-25.3512756988829,26.2253335264758,-11.8824879028166));
#36206=CARTESIAN_POINT('Ctrl Pts',(-25.4469681261721,26.158356969656,-11.8757428998191));
#36207=CARTESIAN_POINT('Ctrl Pts',(-25.580993095657,26.0532674322934,-11.865616769211));
#36208=CARTESIAN_POINT('Ctrl Pts',(-25.622341173741,26.0191468124521,-11.8623912096068));
#36209=CARTESIAN_POINT('Ctrl Pts',(-25.6689114167839,25.9787226694689,-11.8586312177299));
#36210=CARTESIAN_POINT('Ctrl Pts',(-25.6749855153543,25.973410064277,-11.8581382544008));
#36211=CARTESIAN_POINT('Ctrl Pts',(-25.6841550548324,25.965329099659,-11.8573901643942));
#36212=CARTESIAN_POINT('Ctrl Pts',(-25.6872652347003,25.9625774505892,-11.8571357374902));
#36213=CARTESIAN_POINT('Ctrl Pts',(-25.6926357791813,25.9578074669582,-11.8566952111291));
#36214=CARTESIAN_POINT('Ctrl Pts',(-25.6948986368102,25.955791936721,-11.8565092297092));
#36215=CARTESIAN_POINT('Ctrl Pts',(-25.699581876376,25.9516087084781,-11.8561235560615));
#36216=CARTESIAN_POINT('Ctrl Pts',(-25.702001828769,25.9494405364357,-11.855923843951));
#36217=CARTESIAN_POINT('Ctrl Pts',(-25.7078678522686,25.9441688206148,-11.8554387027153));
#36218=CARTESIAN_POINT('Ctrl Pts',(-25.711310504101,25.9410614971876,-11.8551531138208));
#36219=CARTESIAN_POINT('Ctrl Pts',(-25.7241675971189,25.9294062781512,-11.8540832699426));
#36220=CARTESIAN_POINT('Ctrl Pts',(-25.7335380307643,25.9208102051252,-11.8532969690902));
#36221=CARTESIAN_POINT('Ctrl Pts',(-25.8839848030249,25.7811474768813,-11.840564796284));
#36222=CARTESIAN_POINT('Ctrl Pts',(-26.0130596873307,25.6377762435552,-11.8280660194604));
#36223=CARTESIAN_POINT('Ctrl Pts',(-26.2475252882178,25.3251217559499,-11.8019545718791));
#36224=CARTESIAN_POINT('Ctrl Pts',(-26.3515961455029,25.155839979797,-11.7883764777622));
#36225=CARTESIAN_POINT('Ctrl Pts',(-26.4766613551673,24.902770219912,-11.7695444466733));
#36226=CARTESIAN_POINT('Ctrl Pts',(-26.5109199089142,24.8260361159522,-11.7640157667073));
#36227=CARTESIAN_POINT('Ctrl Pts',(-26.5543253674755,24.7176163428053,-11.7565330141741));
#36228=CARTESIAN_POINT('Ctrl Pts',(-26.5660430672305,24.6870020744771,-11.7544556537255));
#36229=CARTESIAN_POINT('Ctrl Pts',(-26.5788720835645,24.6518887543233,-11.7521176072309));
#36230=CARTESIAN_POINT('Ctrl Pts',(-26.5804427086096,24.6475611707439,-11.7518302191037));
#36231=CARTESIAN_POINT('Ctrl Pts',(-26.582795748347,24.6410342013344,-11.7513979446661));
#36232=CARTESIAN_POINT('Ctrl Pts',(-26.5835850469411,24.6388373302832,-11.7512526478649));
#36233=CARTESIAN_POINT('Ctrl Pts',(-26.5850015682601,24.6348811943899,-11.7509913585452));
#36234=CARTESIAN_POINT('Ctrl Pts',(-26.5856296471964,24.6331222457525,-11.7508753147503));
#36235=CARTESIAN_POINT('Ctrl Pts',(-26.5868817555751,24.6296060402704,-11.7506435964224));
#36236=CARTESIAN_POINT('Ctrl Pts',(-26.5875057864466,24.6278487948381,-11.7505279219896));
#36237=CARTESIAN_POINT('Ctrl Pts',(-26.5892612073748,24.6228919627205,-11.7502019868022));
#36238=CARTESIAN_POINT('Ctrl Pts',(-26.5903890734256,24.6196911169978,-11.7499919374142));
#36239=CARTESIAN_POINT('Ctrl Pts',(-26.5950339544138,24.6064423723755,-11.7491242327899));
#36240=CARTESIAN_POINT('Ctrl Pts',(-26.5985062804809,24.5963787106053,-11.7484692162088));
#36241=CARTESIAN_POINT('Ctrl Pts',(-26.6602930171192,24.4143855986378,-11.7366942865875));
#36242=CARTESIAN_POINT('Ctrl Pts',(-26.7040359707909,24.2378198014382,-11.7263958643788));
#36243=CARTESIAN_POINT('Ctrl Pts',(-26.7593992612187,23.8911489492485,-11.7067094764478));
#36244=CARTESIAN_POINT('Ctrl Pts',(-26.7728825408738,23.7219710894425,-11.6973325312428));
#36245=CARTESIAN_POINT('Ctrl Pts',(-26.7730373760849,23.5018494115182,-11.6847662010004));
#36246=CARTESIAN_POINT('Ctrl Pts',(-26.771878018203,23.4511872622335,-11.6818502444379));
#36247=CARTESIAN_POINT('Ctrl Pts',(-26.7648382225419,23.2997749819227,-11.6730349342752));
#36248=CARTESIAN_POINT('Ctrl Pts',(-26.7554204206028,23.1992599943009,-11.6670475195143));
#36249=CARTESIAN_POINT('Ctrl Pts',(-26.7399895831919,23.0900531848866,-11.6603345982499));
#36250=CARTESIAN_POINT('Ctrl Pts',(-26.7386339354106,23.0807528852675,-11.6597612741537));
#36251=CARTESIAN_POINT('Ctrl Pts',(-26.7365634806811,23.0669713611633,-11.6589092293575));
#36252=CARTESIAN_POINT('Ctrl Pts',(-26.7358798515899,23.0624854440236,-11.658631497989));
#36253=CARTESIAN_POINT('Ctrl Pts',(-26.7346946293359,23.0548168951078,-11.6581560534883));
#36254=CARTESIAN_POINT('Ctrl Pts',(-26.7341977321053,23.0516335349656,-11.6579584897021));
#36255=CARTESIAN_POINT('Ctrl Pts',(-26.7332228166025,23.0454486434365,-11.6575742601792));
#36256=CARTESIAN_POINT('Ctrl Pts',(-26.7327453242576,23.0424470321234,-11.6573876113801));
#36257=CARTESIAN_POINT('Ctrl Pts',(-26.7315948250151,23.0352801267279,-11.6569415276695));
#36258=CARTESIAN_POINT('Ctrl Pts',(-26.7309178841769,23.0311154781202,-11.6566819679007));
#36259=CARTESIAN_POINT('Ctrl Pts',(-26.7288700457156,23.0186712175734,-11.6559053527913));
#36260=CARTESIAN_POINT('Ctrl Pts',(-26.7274749911721,23.0103956665729,-11.6553875293497));
#36261=CARTESIAN_POINT('Ctrl Pts',(-26.7152683425993,22.9396714945797,-11.6509502869785));
#36262=CARTESIAN_POINT('Ctrl Pts',(-26.7026497718723,22.8775527446523,-11.6469735072737));
#36263=CARTESIAN_POINT('Ctrl Pts',(-26.666013125833,22.7210116797256,-11.6367384716623));
#36264=CARTESIAN_POINT('Ctrl Pts',(-26.6395313934538,22.6272370678872,-11.6304057951029));
#36265=CARTESIAN_POINT('Ctrl Pts',(-26.5015604862611,22.2116566717861,-11.6014625951904));
#36266=CARTESIAN_POINT('Ctrl Pts',(-26.3437557371046,21.9075793658389,-11.5775911630559));
#36267=CARTESIAN_POINT('Ctrl Pts',(-26.1395697085601,21.6315126944463,-11.5558869418025));
#36268=CARTESIAN_POINT('Ctrl Pts',(-26.1378386876699,21.6291789019263,-11.5557034768337));
#36269=CARTESIAN_POINT('Ctrl Pts',(-26.1287259213196,21.6169275748415,-11.5547404722456));
#36270=CARTESIAN_POINT('Ctrl Pts',(-26.1212901732604,21.6070500545347,-11.5539644077823));
#36271=CARTESIAN_POINT('Ctrl Pts',(-26.1116165001503,21.5943524480285,-11.5529674909093));
#36272=CARTESIAN_POINT('Ctrl Pts',(-26.1094305677089,21.5914931548255,-11.5527430489065));
#36273=CARTESIAN_POINT('Ctrl Pts',(-26.106079599208,21.5871251295831,-11.552400258397));
#36274=CARTESIAN_POINT('Ctrl Pts',(-26.1049180161304,21.5856137713544,-11.5522816659478));
#36275=CARTESIAN_POINT('Ctrl Pts',(-26.1027317979032,21.5827744577653,-11.5520589013934));
#36276=CARTESIAN_POINT('Ctrl Pts',(-26.1017074710651,21.5814462770792,-11.5519547082502));
#36277=CARTESIAN_POINT('Ctrl Pts',(-26.0993461335054,21.5783894158617,-11.5517149314509));
#36278=CARTESIAN_POINT('Ctrl Pts',(-26.0980084034458,21.5766612983333,-11.5515794001561));
#36279=CARTESIAN_POINT('Ctrl Pts',(-26.0942755028341,21.5718491519918,-11.5512020498367));
#36280=CARTESIAN_POINT('Ctrl Pts',(-26.0918764731326,21.5687681004671,-11.5509605056179));
#36281=CARTESIAN_POINT('Ctrl Pts',(-26.0783905485038,21.5515130411277,-11.5496080561479));
#36282=CARTESIAN_POINT('Ctrl Pts',(-26.0671904022372,21.5374273593754,-11.5485051215592));
#36283=CARTESIAN_POINT('Ctrl Pts',(-26.0344135348248,21.4969074761311,-11.5453331139805));
#36284=CARTESIAN_POINT('Ctrl Pts',(-26.0125336022343,21.4707203864211,-11.5432840795104));
#36285=CARTESIAN_POINT('Ctrl Pts',(-25.9265563190034,21.3710781478826,-11.5354692455696));
#36286=CARTESIAN_POINT('Ctrl Pts',(-25.8595502832995,21.3001930534863,-11.529869955924));
#36287=CARTESIAN_POINT('Ctrl Pts',(-25.5382899223414,20.9898307854437,-11.5045779426702));
#36288=CARTESIAN_POINT('Ctrl Pts',(-25.2494218773259,20.7896594059914,-11.4856929433556));
#36289=CARTESIAN_POINT('Ctrl Pts',(-24.9152396361417,20.6307727623383,-11.4633212951716));
#36290=CARTESIAN_POINT('Ctrl Pts',(-24.8963314965093,20.6220067585805,-11.4620550803262));
#36291=CARTESIAN_POINT('Ctrl Pts',(-24.8715917977068,20.6108274356281,-11.4603973473469));
#36292=CARTESIAN_POINT('Ctrl Pts',(-24.8658360122322,20.6082468457493,-11.4600115999601));
#36293=CARTESIAN_POINT('Ctrl Pts',(-24.8569726721231,20.6043042040786,-11.4594174672457));
#36294=CARTESIAN_POINT('Ctrl Pts',(-24.8538704581745,20.6029301238122,-11.4592094952645));
#36295=CARTESIAN_POINT('Ctrl Pts',(-24.8477931353258,20.600249734718,-11.4588020258503));
#36296=CARTESIAN_POINT('Ctrl Pts',(-24.8448182086018,20.5989430209369,-11.4586025426014));
#36297=CARTESIAN_POINT('Ctrl Pts',(-24.8385197517321,20.596187827553,-11.458180152177));
#36298=CARTESIAN_POINT('Ctrl Pts',(-24.8351957452489,20.5947404535176,-11.4579572074583));
#36299=CARTESIAN_POINT('Ctrl Pts',(-24.8257148785467,20.5906312118609,-11.4573212302767));
#36300=CARTESIAN_POINT('Ctrl Pts',(-24.8195521676355,20.5879829645953,-11.4569077329533));
#36301=CARTESIAN_POINT('Ctrl Pts',(-24.8058691274709,20.5821536112319,-11.4559894008776));
#36302=CARTESIAN_POINT('Ctrl Pts',(-24.7983449040709,20.5789818161112,-11.4554842513851));
#36303=CARTESIAN_POINT('Ctrl Pts',(-24.625706606652,20.5069785489612,-11.4438898489663));
#36304=CARTESIAN_POINT('Ctrl Pts',(-24.455187682488,20.451996450664,-11.4323251316667));
#36305=CARTESIAN_POINT('Ctrl Pts',(-23.9740679553818,20.3399845257404,-11.3994472392227));
#36306=CARTESIAN_POINT('Ctrl Pts',(-23.6583168313934,20.3139337483487,-11.3774658963678));
#36307=CARTESIAN_POINT('Ctrl Pts',(-23.327523705548,20.3351668566534,-11.3564861016113));
#36308=CARTESIAN_POINT('Ctrl Pts',(-23.3112412308057,20.3363362831438,-11.3554591774012));
#36309=CARTESIAN_POINT('Ctrl Pts',(-23.2913838105475,20.3379142128347,-11.354214386083));
#36310=CARTESIAN_POINT('Ctrl Pts',(-23.2878001381906,20.3382050178712,-11.3539900407692));
#36311=CARTESIAN_POINT('Ctrl Pts',(-23.2818967585076,20.3386940063553,-11.3536209836586));
#36312=CARTESIAN_POINT('Ctrl Pts',(-23.279576779002,20.3388887062058,-11.3534760762236));
#36313=CARTESIAN_POINT('Ctrl Pts',(-23.2753964832033,20.339244091708,-11.3532152071376));
#36314=CARTESIAN_POINT('Ctrl Pts',(-23.2735360999324,20.3394038797788,-11.3530991949451));
#36315=CARTESIAN_POINT('Ctrl Pts',(-23.2695385087444,20.3397507325356,-11.3528500888909));
#36316=CARTESIAN_POINT('Ctrl Pts',(-23.2674013543699,20.3399383139529,-11.3527170249973));
#36317=CARTESIAN_POINT('Ctrl Pts',(-23.2615552280395,20.3404573208414,-11.352353331752));
#36318=CARTESIAN_POINT('Ctrl Pts',(-23.2578466259508,20.3407930420963,-11.3521229456498));
#36319=CARTESIAN_POINT('Ctrl Pts',(-23.2386781969474,20.3425617649046,-11.3509338288754));
#36320=CARTESIAN_POINT('Ctrl Pts',(-23.2232279461484,20.3441000766881,-11.3499809734857));
#36321=CARTESIAN_POINT('Ctrl Pts',(-23.1352367201633,20.3535036522515,-11.3445832232496));
#36322=CARTESIAN_POINT('Ctrl Pts',(-23.062962282041,20.3637196884551,-11.3402615051862));
#36323=CARTESIAN_POINT('Ctrl Pts',(-22.9091135509578,20.3908242158234,-11.3311840095511));
#36324=CARTESIAN_POINT('Ctrl Pts',(-22.8277217661702,20.4084382096876,-11.3264559130388));
#36325=CARTESIAN_POINT('Ctrl Pts',(-22.5558477524613,20.4784003092772,-11.3106533724097));
#36326=CARTESIAN_POINT('Ctrl Pts',(-22.3695297953643,20.5450886411294,-11.2997819464066));
#36327=CARTESIAN_POINT('Ctrl Pts',(-22.1321173251209,20.6555754981075,-11.2847921199108));
#36328=CARTESIAN_POINT('Ctrl Pts',(-22.0745765457262,20.6844817292307,-11.2810671729841));
#36329=CARTESIAN_POINT('Ctrl Pts',(-22.0071428917295,20.7209273655582,-11.2765681752944));
#36330=CARTESIAN_POINT('Ctrl Pts',(-21.9963770340512,20.7268256796352,-11.2758457740146));
#36331=CARTESIAN_POINT('Ctrl Pts',(-21.9259808504998,20.7659183729809,-11.2710942010826));
#36332=CARTESIAN_POINT('Ctrl Pts',(-21.8673877093177,20.8009362274774,-11.2670068380896));
#36333=CARTESIAN_POINT('Ctrl Pts',(-21.8020335167647,20.8428670065289,-11.2622772292564));
#36334=CARTESIAN_POINT('Ctrl Pts',(-21.794136039208,20.8479829359844,-11.261702799807));
#36335=CARTESIAN_POINT('Ctrl Pts',(-21.7826008177714,20.8555272934198,-11.2608594761728));
#36336=CARTESIAN_POINT('Ctrl Pts',(-21.7789453816287,20.85792868948,-11.2605915964451));
#36337=CARTESIAN_POINT('Ctrl Pts',(-21.7724701390622,20.8622014198005,-11.260115939557));
#36338=CARTESIAN_POINT('Ctrl Pts',(-21.7696483650283,20.8640697722345,-11.2599082748532));
#36339=CARTESIAN_POINT('Ctrl Pts',(-21.7638504152943,20.867921859708,-11.2594807903488));
#36340=CARTESIAN_POINT('Ctrl Pts',(-21.7608745896182,20.869906110874,-11.2592609512581));
#36341=CARTESIAN_POINT('Ctrl Pts',(-21.7532603366251,20.8750015513314,-11.2586973405516));
#36342=CARTESIAN_POINT('Ctrl Pts',(-21.7486266967359,20.8781198427631,-11.2583533004721));
#36343=CARTESIAN_POINT('Ctrl Pts',(-21.7385950569707,20.8849087698546,-11.2576061629992));
#36344=CARTESIAN_POINT('Ctrl Pts',(-21.7332000651039,20.8885837868745,-11.2572028999372));
#36345=CARTESIAN_POINT('Ctrl Pts',(-21.7177118992512,20.8992032130097,-11.256040981323));
#36346=CARTESIAN_POINT('Ctrl Pts',(-21.7076471934574,20.906188761572,-11.2552807580479));
#36347=CARTESIAN_POINT('Ctrl Pts',(-21.6105691107426,20.9743906261362,-11.2478973922628));
#36348=CARTESIAN_POINT('Ctrl Pts',(-21.5266067147818,21.0398163794405,-11.2411116985377));
#36349=CARTESIAN_POINT('Ctrl Pts',(-21.2949796700702,21.2394868389777,-11.2211817427192));
#36350=CARTESIAN_POINT('Ctrl Pts',(-21.1563483875284,21.3834346232592,-11.2076828726417));
#36351=CARTESIAN_POINT('Ctrl Pts',(-20.9161574363896,21.6842195359519,-11.1816406360991));
#36352=CARTESIAN_POINT('Ctrl Pts',(-20.8131096941293,21.838936352253,-11.1691544153083));
#36353=CARTESIAN_POINT('Ctrl Pts',(-20.7185870257793,22.0114503488514,-11.1567620396726));
#36354=CARTESIAN_POINT('Ctrl Pts',(-20.713284006594,22.0212491662408,-11.1560631645944));
#36355=CARTESIAN_POINT('Ctrl Pts',(-20.706402801591,22.0341231779158,-11.1551517070603));
#36356=CARTESIAN_POINT('Ctrl Pts',(-20.704778678292,22.0371735335358,-11.1549362412944));
#36357=CARTESIAN_POINT('Ctrl Pts',(-20.7022798554167,22.0418849631516,-11.1546042122703));
#36358=CARTESIAN_POINT('Ctrl Pts',(-20.701401701886,22.0435441869247,-11.1544874285238));
#36359=CARTESIAN_POINT('Ctrl Pts',(-20.6996535433311,22.0468542304672,-11.1542547467543));
#36360=CARTESIAN_POINT('Ctrl Pts',(-20.6987835275693,22.0485050285722,-11.1541388487279));
#36361=CARTESIAN_POINT('Ctrl Pts',(-20.6968390951136,22.0522022439667,-11.1538796031437));
#36362=CARTESIAN_POINT('Ctrl Pts',(-20.6957654482599,22.0542490573644,-11.1537363052734));
#36363=CARTESIAN_POINT('Ctrl Pts',(-20.692611402426,22.0602777258823,-11.1533148874902));
#36364=CARTESIAN_POINT('Ctrl Pts',(-20.690537115639,22.0642627990928,-11.1530371563274));
#36365=CARTESIAN_POINT('Ctrl Pts',(-20.6748453152691,22.0945640762878,-11.150931606834));
#36366=CARTESIAN_POINT('Ctrl Pts',(-20.6615824102286,22.1210637336271,-11.1491258799801));
#36367=CARTESIAN_POINT('Ctrl Pts',(-20.6177423398682,22.2117618184915,-11.1430532289471));
#36368=CARTESIAN_POINT('Ctrl Pts',(-20.5889231110985,22.2767914951118,-11.1388801528287));
#36369=CARTESIAN_POINT('Ctrl Pts',(-20.4317098374001,22.6658094082142,-11.1146673850531));
#36370=CARTESIAN_POINT('Ctrl Pts',(-20.3544012393794,23.0079261207296,-11.0961163829572));
#36371=CARTESIAN_POINT('Ctrl Pts',(-20.3329972408215,23.3620375716651,-11.0751444405818));
#36372=CARTESIAN_POINT('Ctrl Pts',(-20.332638946003,23.3682654710559,-11.074775149737));
#36373=CARTESIAN_POINT('Ctrl Pts',(-20.3291047356388,23.432973269957,-11.0709334189033));
#36374=CARTESIAN_POINT('Ctrl Pts',(-20.3275055692309,23.491525264142,-11.0674161107802));
#36375=CARTESIAN_POINT('Ctrl Pts',(-20.3275020697863,23.5590868323728,-11.0632996861545));
#36376=CARTESIAN_POINT('Ctrl Pts',(-20.3275393145615,23.5680879494281,-11.0627500831965));
#36377=CARTESIAN_POINT('Ctrl Pts',(-20.3276504210972,23.5814302376652,-11.0619336259482));
#36378=CARTESIAN_POINT('Ctrl Pts',(-20.3276953477459,23.5857716598433,-11.0616676803245));
#36379=CARTESIAN_POINT('Ctrl Pts',(-20.3277907204021,23.5934820312754,-11.0611948582121));
#36380=CARTESIAN_POINT('Ctrl Pts',(-20.3278376770741,23.5968510236899,-11.0609880915805));
#36381=CARTESIAN_POINT('Ctrl Pts',(-20.3279461408953,23.6038457802976,-11.0605584431339));
#36382=CARTESIAN_POINT('Ctrl Pts',(-20.3280084845895,23.6074715251033,-11.060335535339));
#36383=CARTESIAN_POINT('Ctrl Pts',(-20.3281862935942,23.616887836597,-11.0597561083046));
#36384=CARTESIAN_POINT('Ctrl Pts',(-20.3283112489331,23.6226781922177,-11.0593992915113));
#36385=CARTESIAN_POINT('Ctrl Pts',(-20.3286175957744,23.6352970080275,-11.0586205616068));
#36386=CARTESIAN_POINT('Ctrl Pts',(-20.328805089886,23.6421252795975,-11.0581984581353));
#36387=CARTESIAN_POINT('Ctrl Pts',(-20.3294136468704,23.6619864799954,-11.0569685821752));
#36388=CARTESIAN_POINT('Ctrl Pts',(-20.3298920988453,23.6750173972613,-11.0561590105538));
#36389=CARTESIAN_POINT('Ctrl Pts',(-20.3317850816313,23.7192508449693,-11.0534017355312));
#36390=CARTESIAN_POINT('Ctrl Pts',(-20.3335741042706,23.7504348006801,-11.0514423501007));
#36391=CARTESIAN_POINT('Ctrl Pts',(-20.3431774021607,23.883874472474,-11.0429890662033));
#36392=CARTESIAN_POINT('Ctrl Pts',(-20.3554161543005,23.9857423150514,-11.036359679306));
#36393=CARTESIAN_POINT('Ctrl Pts',(-20.4002591410788,24.2513076632075,-11.0186251511043));
#36394=CARTESIAN_POINT('Ctrl Pts',(-20.4407536000566,24.4133543127671,-11.0073331271241));
#36395=CARTESIAN_POINT('Ctrl Pts',(-20.5533437646642,24.7503348948696,-10.9832909540427));
#36396=CARTESIAN_POINT('Ctrl Pts',(-20.628669929482,24.9235817454716,-10.9705877683187));
#36397=CARTESIAN_POINT('Ctrl Pts',(-20.7243003760567,25.099526030514,-10.9579658431494));
#36398=CARTESIAN_POINT('Ctrl Pts',(-20.7299334492485,25.1097570181433,-10.9572330209411));
#36399=CARTESIAN_POINT('Ctrl Pts',(-20.7373367663845,25.1230318717555,-10.9562838748192));
#36400=CARTESIAN_POINT('Ctrl Pts',(-20.7390564617027,25.1261036070177,-10.9560643662478));
#36401=CARTESIAN_POINT('Ctrl Pts',(-20.741707308586,25.1308204250409,-10.9557274894138));
#36402=CARTESIAN_POINT('Ctrl Pts',(-20.7426348731287,25.1324675041543,-10.9556098902253));
#36403=CARTESIAN_POINT('Ctrl Pts',(-20.7444803346888,25.135737762856,-10.9553764708517));
#36404=CARTESIAN_POINT('Ctrl Pts',(-20.7453981861716,25.1373609527406,-10.9552606491788));
#36405=CARTESIAN_POINT('Ctrl Pts',(-20.7474458796603,25.1409749064102,-10.9550028570207));
#36406=CARTESIAN_POINT('Ctrl Pts',(-20.7485764313825,25.1429652588136,-10.9548609336465));
#36407=CARTESIAN_POINT('Ctrl Pts',(-20.7518795295061,25.1487660105674,-10.9544474578528));
#36408=CARTESIAN_POINT('Ctrl Pts',(-20.7540577465721,25.152573200509,-10.9541762722495));
#36409=CARTESIAN_POINT('Ctrl Pts',(-20.7696866439071,25.1797611960014,-10.9522409462619));
#36410=CARTESIAN_POINT('Ctrl Pts',(-20.7834231412716,25.2029776700911,-10.9505950564734));
#36411=CARTESIAN_POINT('Ctrl Pts',(-20.823404865293,25.2686561135142,-10.9459501724487));
#36412=CARTESIAN_POINT('Ctrl Pts',(-20.8503482493828,25.3106861463705,-10.9429913556266));
#36413=CARTESIAN_POINT('Ctrl Pts',(-20.9050930514259,25.3918693509267,-10.9372685578144));
#36414=CARTESIAN_POINT('Ctrl Pts',(-20.9328140951954,25.4310602237635,-10.9345022019202));
#36415=CARTESIAN_POINT('Ctrl Pts',(-20.9823801223373,25.4979151446925,-10.9297501169584));
#36416=CARTESIAN_POINT('Ctrl Pts',(-21.0038219327036,25.5258662750326,-10.9277529211528));
#36417=CARTESIAN_POINT('Ctrl Pts',(-21.1980512743488,25.770642959815,-10.9101179198671));
#36418=CARTESIAN_POINT('Ctrl Pts',(-21.3976749256344,25.96466572331,-10.8949955102029));
#36419=CARTESIAN_POINT('Ctrl Pts',(-21.6251372096428,26.1348405511653,-10.8782883019415));
#36420=CARTESIAN_POINT('Ctrl Pts',(-21.6306203456497,26.1389156041942,-10.877885920855));
#36421=CARTESIAN_POINT('Ctrl Pts',(-21.6916017370523,26.1839365311524,-10.8734145388434));
#36422=CARTESIAN_POINT('Ctrl Pts',(-21.7483842412458,26.2231056451519,-10.8692848236058));
#36423=CARTESIAN_POINT('Ctrl Pts',(-21.8143135424199,26.2655282946416,-10.8645096481306));
#36424=CARTESIAN_POINT('Ctrl Pts',(-21.8222729718332,26.2706005390368,-10.8639334865715));
#36425=CARTESIAN_POINT('Ctrl Pts',(-21.8339577650372,26.2779748439592,-10.8630880938868));
#36426=CARTESIAN_POINT('Ctrl Pts',(-21.8376657736613,26.2803044240202,-10.8628198843771));
#36427=CARTESIAN_POINT('Ctrl Pts',(-21.8442485226174,26.2844213893906,-10.8623438465494));
#36428=CARTESIAN_POINT('Ctrl Pts',(-21.8471213583685,26.2862118200774,-10.8621361312973));
#36429=CARTESIAN_POINT('Ctrl Pts',(-21.8530340518322,26.2898838527492,-10.8617086972607));
#36430=CARTESIAN_POINT('Ctrl Pts',(-21.8560742292637,26.2917649287298,-10.8614889594392));
#36431=CARTESIAN_POINT('Ctrl Pts',(-21.8638571161662,26.2965626134129,-10.8609265252893));
#36432=CARTESIAN_POINT('Ctrl Pts',(-21.8686042510996,26.2994719885973,-10.8605835631688));
#36433=CARTESIAN_POINT('Ctrl Pts',(-21.878916981061,26.3057556438926,-10.8598386963904));
#36434=CARTESIAN_POINT('Ctrl Pts',(-21.8844852977342,26.3091253894773,-10.8594366268668));
#36435=CARTESIAN_POINT('Ctrl Pts',(-21.9005219436543,26.3187639428006,-10.8582789918572));
#36436=CARTESIAN_POINT('Ctrl Pts',(-21.9110156314546,26.3249901453856,-10.8575218726729));
#36437=CARTESIAN_POINT('Ctrl Pts',(-21.9461964382207,26.3455946930952,-10.8549847189624));
#36438=CARTESIAN_POINT('Ctrl Pts',(-21.971038796963,26.3597040165143,-10.8531949987811));
#36439=CARTESIAN_POINT('Ctrl Pts',(-22.0221954802462,26.38786578011,-10.8495124069177));
#36440=CARTESIAN_POINT('Ctrl Pts',(-22.0485217771435,26.4018856884949,-10.8476187983523));
#36441=CARTESIAN_POINT('Ctrl Pts',(-22.0750360250409,26.4155367795477,-10.8457129588805));
#36442=CARTESIAN_POINT('Origin',(-23.5502525316942,23.5502525316942,-77.3107734492734));
#36443=CARTESIAN_POINT('',(-22.075036015341,26.4155367745536,-9.34735996012824));
#36444=CARTESIAN_POINT('',(-22.0750360153461,26.4155367745563,-9.5929697214734));
#36445=CARTESIAN_POINT('',(-22.0750360153461,26.4155367745563,-77.3107734492734));
#36446=CARTESIAN_POINT('Ctrl Pts',(-22.075036015341,26.4155367745536,-9.34735996012824));
#36447=CARTESIAN_POINT('Ctrl Pts',(-22.0747390535194,26.4153838811766,-9.34738251109341));
#36448=CARTESIAN_POINT('Ctrl Pts',(-22.074442114912,26.4152309413477,-9.34740506162473));
#36449=CARTESIAN_POINT('Ctrl Pts',(-21.9846698447257,26.3689755900912,-9.35422307522353));
#36450=CARTESIAN_POINT('Ctrl Pts',(-21.897397509723,26.3187036640452,-9.36097361240509));
#36451=CARTESIAN_POINT('Ctrl Pts',(-21.7782939954875,26.2424526342591,-9.37023478749855));
#36452=CARTESIAN_POINT('Ctrl Pts',(-21.7443895201671,26.2198288196812,-9.3728766708831));
#36453=CARTESIAN_POINT('Ctrl Pts',(-21.6862415807607,26.179412874206,-9.37740532370636));
#36454=CARTESIAN_POINT('Ctrl Pts',(-21.6618015139228,26.1619136594497,-9.37930800960738));
#36455=CARTESIAN_POINT('Ctrl Pts',(-21.6339917551444,26.1414071768864,-9.38146880448542));
#36456=CARTESIAN_POINT('Ctrl Pts',(-21.630380282287,26.1387324534987,-9.38174932972123));
#36457=CARTESIAN_POINT('Ctrl Pts',(-21.624904404594,26.1346591529001,-9.38217453312394));
#36458=CARTESIAN_POINT('Ctrl Pts',(-21.6230359214072,26.1332661072253,-9.38231959624138));
#36459=CARTESIAN_POINT('Ctrl Pts',(-21.6196731006669,26.1307532795934,-9.3825806272189));
#36460=CARTESIAN_POINT('Ctrl Pts',(-21.6181782286314,26.1296342283258,-9.38269664592237));
#36461=CARTESIAN_POINT('Ctrl Pts',(-21.6151910482777,26.1273939911176,-9.38292844961065));
#36462=CARTESIAN_POINT('Ctrl Pts',(-21.6136987473629,26.1262728124598,-9.38304423427671));
#36463=CARTESIAN_POINT('Ctrl Pts',(-21.6094885644167,26.1231039393174,-9.38337084826195));
#36464=CARTESIAN_POINT('Ctrl Pts',(-21.6067729400595,26.1210532278869,-9.38358146475285));
#36465=CARTESIAN_POINT('Ctrl Pts',(-21.5955224347469,26.1125293621777,-9.38445382326191));
#36466=CARTESIAN_POINT('Ctrl Pts',(-21.5870164786845,26.1060178800281,-9.38511289173423));
#36467=CARTESIAN_POINT('Ctrl Pts',(-21.4442423141574,25.9955879750525,-9.39617036879566));
#36468=CARTESIAN_POINT('Ctrl Pts',(-21.3183385674023,25.8812442180018,-9.40585086607581));
#36469=CARTESIAN_POINT('Ctrl Pts',(-21.0837018777555,25.6316195088344,-9.42510198676223));
#36470=CARTESIAN_POINT('Ctrl Pts',(-20.975700453274,25.4964389287546,-9.43464376881431));
#36471=CARTESIAN_POINT('Ctrl Pts',(-20.8154770566981,25.2590634167451,-9.45095020197856));
#36472=CARTESIAN_POINT('Ctrl Pts',(-20.7569321223013,25.1615839265824,-9.45753208671471));
#36473=CARTESIAN_POINT('Ctrl Pts',(-20.6801694375884,25.0169668922129,-9.46728276647328));
#36474=CARTESIAN_POINT('Ctrl Pts',(-20.6577147213345,24.9721711549148,-9.47030061012103));
#36475=CARTESIAN_POINT('Ctrl Pts',(-20.6329331207617,24.9197150798299,-9.4738381028785));
#36476=CARTESIAN_POINT('Ctrl Pts',(-20.6295784043342,24.9125457659714,-9.47432165391052));
#36477=CARTESIAN_POINT('Ctrl Pts',(-20.6244987995178,24.9015852106788,-9.47506105062484));
#36478=CARTESIAN_POINT('Ctrl Pts',(-20.6227547759665,24.897802827819,-9.47531623408223));
#36479=CARTESIAN_POINT('Ctrl Pts',(-20.6197539517938,24.8912614158912,-9.47575760587462));
#36480=CARTESIAN_POINT('Ctrl Pts',(-20.6184937000125,24.8885039681021,-9.47594367479258));
#36481=CARTESIAN_POINT('Ctrl Pts',(-20.6158932303915,24.882792802761,-9.47632908813932));
#36482=CARTESIAN_POINT('Ctrl Pts',(-20.6145535773565,24.879838832965,-9.47652845178942));
#36483=CARTESIAN_POINT('Ctrl Pts',(-20.6113176049361,24.8726746958927,-9.47701200465124));
#36484=CARTESIAN_POINT('Ctrl Pts',(-20.6094258739274,24.8684624742697,-9.47729635145109));
#36485=CARTESIAN_POINT('Ctrl Pts',(-20.6024112757544,24.8527531724368,-9.47835696069549));
#36486=CARTESIAN_POINT('Ctrl Pts',(-20.5973467762154,24.8412302934675,-9.47913522400431));
#36487=CARTESIAN_POINT('Ctrl Pts',(-20.511514307439,24.642794314304,-9.49254377675888));
#36488=CARTESIAN_POINT('Ctrl Pts',(-20.4485872706461,24.448707695008,-9.50579587912776));
#36489=CARTESIAN_POINT('Ctrl Pts',(-20.3686898450663,24.0895205169718,-9.530443807561));
#36490=CARTESIAN_POINT('Ctrl Pts',(-20.3453248601385,23.9265335490469,-9.54165917316333));
#36491=CARTESIAN_POINT('Ctrl Pts',(-20.3285343974546,23.6721162340426,-9.55877587430546));
#36492=CARTESIAN_POINT('Ctrl Pts',(-20.3263818166247,23.5815353264292,-9.56479027668491));
#36493=CARTESIAN_POINT('Ctrl Pts',(-20.3289403104488,23.4424542564692,-9.57379463976762));
#36494=CARTESIAN_POINT('Ctrl Pts',(-20.3309289690499,23.3939536662682,-9.57689133459828));
#36495=CARTESIAN_POINT('Ctrl Pts',(-20.3343289991591,23.3405427262172,-9.58024032595217));
#36496=CARTESIAN_POINT('Ctrl Pts',(-20.3346569432289,23.335572812433,-9.58055136525348));
#36497=CARTESIAN_POINT('Ctrl Pts',(-20.3351620663596,23.3281787380981,-9.58101322711576));
#36498=CARTESIAN_POINT('Ctrl Pts',(-20.3353304663261,23.3257540154612,-9.58116454166228));
#36499=CARTESIAN_POINT('Ctrl Pts',(-20.3356216094619,23.3216294779106,-9.58142168733151));
#36500=CARTESIAN_POINT('Ctrl Pts',(-20.3357429578991,23.3199295694686,-9.58152759765232));
#36501=CARTESIAN_POINT('Ctrl Pts',(-20.3359940496529,23.3164510057501,-9.58174417829698));
#36502=CARTESIAN_POINT('Ctrl Pts',(-20.3361239206669,23.3146723654604,-9.58185484107985));
#36503=CARTESIAN_POINT('Ctrl Pts',(-20.3364387004545,23.3104100343879,-9.58211984809862));
#36504=CARTESIAN_POINT('Ctrl Pts',(-20.3366250124269,23.3079264437729,-9.58227411269627));
#36505=CARTESIAN_POINT('Ctrl Pts',(-20.3373073214612,23.2989702624481,-9.58282987742307));
#36506=CARTESIAN_POINT('Ctrl Pts',(-20.3378200000249,23.2924989012617,-9.58323044113451));
#36507=CARTESIAN_POINT('Ctrl Pts',(-20.3461491522941,23.1912497306722,-9.58948238160495));
#36508=CARTESIAN_POINT('Ctrl Pts',(-20.3581384015592,23.096851044737,-9.59510353979885));
#36509=CARTESIAN_POINT('Ctrl Pts',(-20.4035777894445,22.8330912459621,-9.61056684772774));
#36510=CARTESIAN_POINT('Ctrl Pts',(-20.4464751059084,22.6656873590403,-9.62010688841638));
#36511=CARTESIAN_POINT('Ctrl Pts',(-20.5470761590138,22.3730571221707,-9.63742849064915));
#36512=CARTESIAN_POINT('Ctrl Pts',(-20.5997818017243,22.2465747241142,-9.64514636155865));
#36513=CARTESIAN_POINT('Ctrl Pts',(-20.6881973355374,22.0674472030933,-9.65675171250586));
#36514=CARTESIAN_POINT('Ctrl Pts',(-20.7176719379784,22.0118904072639,-9.66045042146399));
#36515=CARTESIAN_POINT('Ctrl Pts',(-20.7708824173946,21.9183138468992,-9.66687813589731));
#36516=CARTESIAN_POINT('Ctrl Pts',(-20.7938211840708,21.879860954121,-9.66957889943404));
#36517=CARTESIAN_POINT('Ctrl Pts',(-20.8216432702251,21.8353564389058,-9.67277976901697));
#36518=CARTESIAN_POINT('Ctrl Pts',(-20.8257573184495,21.8288278478321,-9.67325124469969));
#36519=CARTESIAN_POINT('Ctrl Pts',(-20.8320992698812,21.818843477422,-9.67397526689835));
#36520=CARTESIAN_POINT('Ctrl Pts',(-20.8343104245528,21.8153770496123,-9.67422719008157));
#36521=CARTESIAN_POINT('Ctrl Pts',(-20.8383330506354,21.8090973154977,-9.67468457956155));
#36522=CARTESIAN_POINT('Ctrl Pts',(-20.8401422840608,21.8062825766283,-9.67488996213777));
#36523=CARTESIAN_POINT('Ctrl Pts',(-20.8440390567054,21.8002408283811,-9.67533160513456));
#36524=CARTESIAN_POINT('Ctrl Pts',(-20.8461279898384,21.7970147281226,-9.67556791749557));
#36525=CARTESIAN_POINT('Ctrl Pts',(-20.8517487772766,21.7883680557496,-9.67620260630327));
#36526=CARTESIAN_POINT('Ctrl Pts',(-20.8552911780625,21.7829543902832,-9.6766013779747));
#36527=CARTESIAN_POINT('Ctrl Pts',(-20.8714722502908,21.7583874838224,-9.67841736847568));
#36528=CARTESIAN_POINT('Ctrl Pts',(-20.8842987166384,21.7393592830675,-9.67984165159534));
#36529=CARTESIAN_POINT('Ctrl Pts',(-20.9042960531253,21.7103659765101,-9.6820396668591));
#36530=CARTESIAN_POINT('Ctrl Pts',(-20.9113226617626,21.70030189525,-9.6828078612671));
#36531=CARTESIAN_POINT('Ctrl Pts',(-20.9214112362097,21.6860266573506,-9.68390501421969));
#36532=CARTESIAN_POINT('Ctrl Pts',(-20.9244262424308,21.6817823110277,-9.68423217595527));
#36533=CARTESIAN_POINT('Ctrl Pts',(-20.9285214914673,21.6760467517025,-9.6846755792827));
#36534=CARTESIAN_POINT('Ctrl Pts',(-20.9295927593767,21.6745491140992,-9.68479147830318));
#36535=CARTESIAN_POINT('Ctrl Pts',(-20.9333950427281,21.6692431199714,-9.68520252397582));
#36536=CARTESIAN_POINT('Ctrl Pts',(-20.9361330710183,21.6654398169953,-9.68549793770175));
#36537=CARTESIAN_POINT('Ctrl Pts',(-20.9400733968353,21.6599915449934,-9.6859222421535));
#36538=CARTESIAN_POINT('Ctrl Pts',(-20.9412689831607,21.6583417099727,-9.68605087713408));
#36539=CARTESIAN_POINT('Ctrl Pts',(-20.946536609641,21.6510872009053,-9.68661715139819));
#36540=CARTESIAN_POINT('Ctrl Pts',(-20.9506251277027,21.6454945639614,-9.68705541680821));
#36541=CARTESIAN_POINT('Ctrl Pts',(-20.9576949891945,21.6358889446205,-9.68781112252777));
#36542=CARTESIAN_POINT('Ctrl Pts',(-20.9606677080853,21.6318696200805,-9.68812823470617));
#36543=CARTESIAN_POINT('Ctrl Pts',(-20.9689327041858,21.6207489821766,-9.68900811656925));
#36544=CARTESIAN_POINT('Ctrl Pts',(-20.9742448912833,21.6136625819231,-9.68957163732889));
#36545=CARTESIAN_POINT('Ctrl Pts',(-20.9902763494368,21.5924594647369,-9.69126628620316));
#36546=CARTESIAN_POINT('Ctrl Pts',(-21.0010828125483,21.5784093659837,-9.69240067716879));
#36547=CARTESIAN_POINT('Ctrl Pts',(-21.0262806186788,21.5462016008251,-9.69502770223168));
#36548=CARTESIAN_POINT('Ctrl Pts',(-21.0407528471351,21.5281087083611,-9.6965232796239));
#36549=CARTESIAN_POINT('Ctrl Pts',(-21.0955479468654,21.4610992005697,-9.70213690134174));
#36550=CARTESIAN_POINT('Ctrl Pts',(-21.1371144419831,21.4132218745046,-9.70629882116239));
#36551=CARTESIAN_POINT('Ctrl Pts',(-21.3265191106306,21.2076371705,-9.72483299511883));
#36552=CARTESIAN_POINT('Ctrl Pts',(-21.4885934981391,21.0638115873531,-9.73964224288625));
#36553=CARTESIAN_POINT('Ctrl Pts',(-21.7325980098313,20.8876513193275,-9.75978129155776));
#36554=CARTESIAN_POINT('Ctrl Pts',(-21.803313444654,20.8407287259957,-9.76539032347615));
#36555=CARTESIAN_POINT('Ctrl Pts',(-21.911519628833,20.7749292336555,-9.77355446550235));
#36556=CARTESIAN_POINT('Ctrl Pts',(-21.9476574030216,20.753905949627,-9.77621448616853));
#36557=CARTESIAN_POINT('Ctrl Pts',(-21.9885050780738,20.7311947527816,-9.77913888715837));
#36558=CARTESIAN_POINT('Ctrl Pts',(-21.992819598548,20.7288088357721,-9.77944676284489));
#36559=CARTESIAN_POINT('Ctrl Pts',(-21.9992604264859,20.7252663528676,-9.77990483953177));
#36560=CARTESIAN_POINT('Ctrl Pts',(-22.0013825635011,20.7241022804333,-9.78005552085674));
#36561=CARTESIAN_POINT('Ctrl Pts',(-22.004999696645,20.7221234439255,-9.78031193102136));
#36562=CARTESIAN_POINT('Ctrl Pts',(-22.0064940271831,20.7213074737059,-9.78041773790236));
#36563=CARTESIAN_POINT('Ctrl Pts',(-22.0095578730891,20.7196376296129,-9.78063442293591));
#36564=CARTESIAN_POINT('Ctrl Pts',(-22.0111274486605,20.7187838785471,-9.78074529307251));
#36565=CARTESIAN_POINT('Ctrl Pts',(-22.0148976076577,20.7167372087553,-9.78101128314075));
#36566=CARTESIAN_POINT('Ctrl Pts',(-22.0170988765896,20.7155455454201,-9.78116632210662));
#36567=CARTESIAN_POINT('Ctrl Pts',(-22.025083306796,20.7112351719233,-9.78172773152173));
#36568=CARTESIAN_POINT('Ctrl Pts',(-22.0308746651521,20.7081315571201,-9.78213314045711));
#36569=CARTESIAN_POINT('Ctrl Pts',(-22.1254957442279,20.6577955730134,-9.78872821189812));
#36570=CARTESIAN_POINT('Ctrl Pts',(-22.2164904522242,20.61472488069,-9.79466012494776));
#36571=CARTESIAN_POINT('Ctrl Pts',(-22.5520284211504,20.4747357422122,-9.81560844117375));
#36572=CARTESIAN_POINT('Ctrl Pts',(-22.8061803318503,20.4035672265499,-9.82984096156313));
#36573=CARTESIAN_POINT('Ctrl Pts',(-23.166379967222,20.3488413569926,-9.85068814070944));
#36574=CARTESIAN_POINT('Ctrl Pts',(-23.2672455667249,20.3383534202546,-9.8565856651163));
#36575=CARTESIAN_POINT('Ctrl Pts',(-23.4155357047346,20.3299738430851,-9.86544377773439));
#36576=CARTESIAN_POINT('Ctrl Pts',(-23.4626906719376,20.328346881503,-9.86828780846819));
#36577=CARTESIAN_POINT('Ctrl Pts',(-23.5176815465956,20.3276576394121,-9.87164146282653));
#36578=CARTESIAN_POINT('Ctrl Pts',(-23.5255008203747,20.3275880968017,-9.87211919510026));
#36579=CARTESIAN_POINT('Ctrl Pts',(-23.537453797147,20.327525295042,-9.87285083661871));
#36580=CARTESIAN_POINT('Ctrl Pts',(-23.5415874010033,20.3275115298879,-9.87310410183783));
#36581=CARTESIAN_POINT('Ctrl Pts',(-23.5490378281936,20.3275010537897,-9.8735610383569));
#36582=CARTESIAN_POINT('Ctrl Pts',(-23.5523546470086,20.3275015104671,-9.87376462044286));
#36583=CARTESIAN_POINT('Ctrl Pts',(-23.5594877326846,20.3275135044656,-9.8742027883526));
#36584=CARTESIAN_POINT('Ctrl Pts',(-23.5633039884165,20.327526700067,-9.87443742593883));
#36585=CARTESIAN_POINT('Ctrl Pts',(-23.5736362062145,20.3275807789736,-9.87507327412818));
#36586=CARTESIAN_POINT('Ctrl Pts',(-23.5801520566657,20.3276346456541,-9.87547489178656));
#36587=CARTESIAN_POINT('Ctrl Pts',(-23.6093342788254,20.327964408197,-9.87727645487755));
#36588=CARTESIAN_POINT('Ctrl Pts',(-23.6319970813382,20.3284596783319,-9.87868327024003));
#36589=CARTESIAN_POINT('Ctrl Pts',(-23.6670701360143,20.3295964534935,-9.88087286852073));
#36590=CARTESIAN_POINT('Ctrl Pts',(-23.6794853811566,20.3300707370793,-9.88165035446542));
#36591=CARTESIAN_POINT('Ctrl Pts',(-23.6972252015651,20.3308511841064,-9.88276477548147));
#36592=CARTESIAN_POINT('Ctrl Pts',(-23.7025523524905,20.3310987971587,-9.88309987888756));
#36593=CARTESIAN_POINT('Ctrl Pts',(-23.7097512048707,20.3314513185223,-9.88355333299904));
#36594=CARTESIAN_POINT('Ctrl Pts',(-23.7116234875956,20.3315446401281,-9.8836713236013));
#36595=CARTESIAN_POINT('Ctrl Pts',(-23.7198280824767,20.3319607647021,-9.88418861983742));
#36596=CARTESIAN_POINT('Ctrl Pts',(-23.7261594820091,20.3323006195582,-9.88458845294889));
#36597=CARTESIAN_POINT('Ctrl Pts',(-23.7393456647753,20.3330474553642,-9.88542251391946));
#36598=CARTESIAN_POINT('Ctrl Pts',(-23.7462002268581,20.3334576647911,-9.88585683928375));
#36599=CARTESIAN_POINT('Ctrl Pts',(-23.7568096402509,20.3341266185862,-9.88653025964454));
#36600=CARTESIAN_POINT('Ctrl Pts',(-23.7605654665859,20.3343700404819,-9.88676888475878));
#36601=CARTESIAN_POINT('Ctrl Pts',(-23.7737523594959,20.3352479069463,-9.88760751308457));
#36602=CARTESIAN_POINT('Ctrl Pts',(-23.7831809850994,20.3359172593937,-9.88820857613902));
#36603=CARTESIAN_POINT('Ctrl Pts',(-24.0719187312115,20.3576922755111,-9.9066596858067));
#36604=CARTESIAN_POINT('Ctrl Pts',(-24.3472515408912,20.4150792757007,-9.92568629299455));
#36605=CARTESIAN_POINT('Ctrl Pts',(-24.7633295307349,20.5602068282034,-9.95542712266374));
#36606=CARTESIAN_POINT('Ctrl Pts',(-24.9108788538933,20.6243955747775,-9.96615011634887));
#36607=CARTESIAN_POINT('Ctrl Pts',(-25.0624403420376,20.704287229215,-9.97693631001475));
#36608=CARTESIAN_POINT('Ctrl Pts',(-25.0718160400266,20.7092887912853,-9.97760253609404));
#36609=CARTESIAN_POINT('Ctrl Pts',(-25.0840281774851,20.7158812781397,-9.97846881598465));
#36610=CARTESIAN_POINT('Ctrl Pts',(-25.0868870473853,20.7174301758083,-9.97867150486809));
#36611=CARTESIAN_POINT('Ctrl Pts',(-25.0915487623728,20.7199649643391,-9.97900183002843));
#36612=CARTESIAN_POINT('Ctrl Pts',(-25.0933530083647,20.7209482526204,-9.97912963271979));
#36613=CARTESIAN_POINT('Ctrl Pts',(-25.0968107425152,20.7228369596891,-9.97937447178313));
#36614=CARTESIAN_POINT('Ctrl Pts',(-25.0984643716151,20.7237421009656,-9.97949152512684));
#36615=CARTESIAN_POINT('Ctrl Pts',(-25.1022591203435,20.7258235488114,-9.97976005206337));
#36616=CARTESIAN_POINT('Ctrl Pts',(-25.1043997023312,20.727000842125,-9.97991146194047));
#36617=CARTESIAN_POINT('Ctrl Pts',(-25.1111657035001,20.7307320849471,-9.98038984703385));
#36618=CARTESIAN_POINT('Ctrl Pts',(-25.1157862121243,20.733294992802,-9.98071624845048));
#36619=CARTESIAN_POINT('Ctrl Pts',(-25.1543543425834,20.7548122005366,-9.98343853891612));
#36620=CARTESIAN_POINT('Ctrl Pts',(-25.1879645355018,20.7743690707541,-9.98579638434052));
#36621=CARTESIAN_POINT('Ctrl Pts',(-25.2237875798539,20.796090760667,-9.98830280071763));
#36622=CARTESIAN_POINT('Ctrl Pts',(-25.2263586099929,20.7976546618934,-9.9884826494509));
#36623=CARTESIAN_POINT('Ctrl Pts',(-25.2305181845883,20.8001928285594,-9.98877356563378));
#36624=CARTESIAN_POINT('Ctrl Pts',(-25.2321080751696,20.8011648710305,-9.98888474797332));
#36625=CARTESIAN_POINT('Ctrl Pts',(-25.328339293603,20.8601143579881,-9.99561354959413));
#36626=CARTESIAN_POINT('Ctrl Pts',(-25.4199324553258,20.9229464103117,-10.0019768269906));
#36627=CARTESIAN_POINT('Ctrl Pts',(-25.5671900831203,21.0355730070908,-10.0124509496099));
#36628=CARTESIAN_POINT('Ctrl Pts',(-25.6246912956887,21.0827934296245,-10.0166087227454));
#36629=CARTESIAN_POINT('Ctrl Pts',(-25.8034326485388,21.240245449707,-10.0299189994371));
#36630=CARTESIAN_POINT('Ctrl Pts',(-25.9179173118541,21.3577397371085,-10.0390594299042));
#36631=CARTESIAN_POINT('Ctrl Pts',(-26.0747348527825,21.5453530286679,-10.0531902584915));
#36632=CARTESIAN_POINT('Ctrl Pts',(-26.1241530730788,21.6092044963813,-10.0579260128179));
#36633=CARTESIAN_POINT('Ctrl Pts',(-26.1949155845257,21.7080942925147,-10.06520144191));
#36634=CARTESIAN_POINT('Ctrl Pts',(-26.2180753396393,21.7417971487987,-10.0676710064229));
#36635=CARTESIAN_POINT('Ctrl Pts',(-26.2447238609835,21.7822032444536,-10.0706235045224));
#36636=CARTESIAN_POINT('Ctrl Pts',(-26.2488389391339,21.7884905084494,-10.0710826841287));
#36637=CARTESIAN_POINT('Ctrl Pts',(-26.2551299220064,21.7981760071205,-10.0717897108842));
#36638=CARTESIAN_POINT('Ctrl Pts',(-26.2573215149605,21.8015640619583,-10.0720369706387));
#36639=CARTESIAN_POINT('Ctrl Pts',(-26.2612996729755,21.8077394266714,-10.0724875370242));
#36640=CARTESIAN_POINT('Ctrl Pts',(-26.2630883194998,21.8105253945555,-10.0726907656131));
#36641=CARTESIAN_POINT('Ctrl Pts',(-26.2666968242171,21.8161650415384,-10.0731020817524));
#36642=CARTESIAN_POINT('Ctrl Pts',(-26.2685164860016,21.8190188408053,-10.0733101762752));
#36643=CARTESIAN_POINT('Ctrl Pts',(-26.2736927005022,21.8271650453788,-10.0739040697769));
#36644=CARTESIAN_POINT('Ctrl Pts',(-26.2770383020341,21.8324643607146,-10.0742902748534));
#36645=CARTESIAN_POINT('Ctrl Pts',(-26.2912617880296,21.8551401198139,-10.0759422882866));
#36646=CARTESIAN_POINT('Ctrl Pts',(-26.3019890038667,21.8726100821049,-10.0772136507182));
#36647=CARTESIAN_POINT('Ctrl Pts',(-26.4995866551252,22.2014050583506,-10.1011196089587));
#36648=CARTESIAN_POINT('Ctrl Pts',(-26.6326452279545,22.5419521747354,-10.1259601704792));
#36649=CARTESIAN_POINT('Ctrl Pts',(-26.732547040215,23.0248274841494,-10.159025998282));
#36650=CARTESIAN_POINT('Ctrl Pts',(-26.7511783079503,23.153827383647,-10.1676132462524));
#36651=CARTESIAN_POINT('Ctrl Pts',(-26.7626162805975,23.2916004492935,-10.1762937282554));
#36652=CARTESIAN_POINT('Ctrl Pts',(-26.7632493920115,23.2995875483942,-10.1767952067479));
#36653=CARTESIAN_POINT('Ctrl Pts',(-26.7640728546898,23.310492150462,-10.177477393871));
#36654=CARTESIAN_POINT('Ctrl Pts',(-26.7642890251168,23.3134075865963,-10.1776595414301));
#36655=CARTESIAN_POINT('Ctrl Pts',(-26.764644058261,23.3182858352149,-10.1779639120214));
#36656=CARTESIAN_POINT('Ctrl Pts',(-26.7647850903777,23.3202484805264,-10.1780862578335));
#36657=CARTESIAN_POINT('Ctrl Pts',(-26.765059292106,23.3241138710123,-10.1783269965325));
#36658=CARTESIAN_POINT('Ctrl Pts',(-26.7651925700087,23.3260166052245,-10.1784453953639));
#36659=CARTESIAN_POINT('Ctrl Pts',(-26.7654826872429,23.3302118771472,-10.178706220523));
#36660=CARTESIAN_POINT('Ctrl Pts',(-26.7656387642892,23.3325044705812,-10.1788486035922));
#36661=CARTESIAN_POINT('Ctrl Pts',(-26.7661753359414,23.3405124777155,-10.1793454276422));
#36662=CARTESIAN_POINT('Ctrl Pts',(-26.766543047716,23.3462287809585,-10.17969914965));
#36663=CARTESIAN_POINT('Ctrl Pts',(-26.7701038148466,23.4039864428252,-10.1832641191217));
#36664=CARTESIAN_POINT('Ctrl Pts',(-26.7720489639991,23.4561006919476,-10.1864065994673));
#36665=CARTESIAN_POINT('Ctrl Pts',(-26.7727859288459,23.5126316309057,-10.1897571632614));
#36666=CARTESIAN_POINT('Ctrl Pts',(-26.7728341783268,23.5170206328173,-10.1900169169239));
#36667=CARTESIAN_POINT('Ctrl Pts',(-26.7729151238169,23.5260647172103,-10.1905514123317));
#36668=CARTESIAN_POINT('Ctrl Pts',(-26.7729467005438,23.5307198017021,-10.1908261082017));
#36669=CARTESIAN_POINT('Ctrl Pts',(-26.772988734737,23.5398250691909,-10.1913626260476));
#36670=CARTESIAN_POINT('Ctrl Pts',(-26.7730000611601,23.5442752352923,-10.1916244815034));
#36671=CARTESIAN_POINT('Ctrl Pts',(-26.7730410078804,23.630688050694,-10.1967023026275));
#36672=CARTESIAN_POINT('Ctrl Pts',(-26.7699530515089,23.7126276716292,-10.2013978952144));
#36673=CARTESIAN_POINT('Ctrl Pts',(-26.7373615528694,24.1416612933297,-10.2257532562892));
#36674=CARTESIAN_POINT('Ctrl Pts',(-26.6548659564374,24.4823478884039,-10.2445976408222));
#36675=CARTESIAN_POINT('Ctrl Pts',(-26.5113575270721,24.8224192390291,-10.2669140183395));
#36676=CARTESIAN_POINT('Ctrl Pts',(-26.5030783615903,24.8415195496261,-10.2681787942277));
#36677=CARTESIAN_POINT('Ctrl Pts',(-26.4920515154291,24.8662981434579,-10.269834889117));
#36678=CARTESIAN_POINT('Ctrl Pts',(-26.4894712680562,24.8720507507399,-10.2702204513702));
#36679=CARTESIAN_POINT('Ctrl Pts',(-26.485476833354,24.8808867294941,-10.2708143537528));
#36680=CARTESIAN_POINT('Ctrl Pts',(-26.4840746205018,24.8839755241083,-10.2710222810232));
#36681=CARTESIAN_POINT('Ctrl Pts',(-26.4812944263676,24.8900741362478,-10.271433447829));
#36682=CARTESIAN_POINT('Ctrl Pts',(-26.4799166791037,24.8930840563509,-10.2716366790894));
#36683=CARTESIAN_POINT('Ctrl Pts',(-26.4768541329118,24.8997475548306,-10.2720872765549));
#36684=CARTESIAN_POINT('Ctrl Pts',(-26.4751671266824,24.9034001073525,-10.2723347188659));
#36685=CARTESIAN_POINT('Ctrl Pts',(-26.4703328160856,24.9138156357279,-10.2730416111586));
#36686=CARTESIAN_POINT('Ctrl Pts',(-26.4671688801472,24.9205708234068,-10.2735016369658));
#36687=CARTESIAN_POINT('Ctrl Pts',(-26.4469553181897,24.9633407388018,-10.2764242207016));
#36688=CARTESIAN_POINT('Ctrl Pts',(-26.4292630706707,24.9990463061302,-10.27890906874));
#36689=CARTESIAN_POINT('Ctrl Pts',(-26.3747472386604,25.1041234174917,-10.2863604748528));
#36690=CARTESIAN_POINT('Ctrl Pts',(-26.3360472482928,25.1724828424994,-10.2913920875343));
#36691=CARTESIAN_POINT('Ctrl Pts',(-26.215888854951,25.3677292585338,-10.3063138446229));
#36692=CARTESIAN_POINT('Ctrl Pts',(-26.1279844275276,25.4903887584476,-10.3164081400788));
#36693=CARTESIAN_POINT('Ctrl Pts',(-25.9631484643416,25.6893268042344,-10.3338711529497));
#36694=CARTESIAN_POINT('Ctrl Pts',(-25.8903565521599,25.768724801521,-10.3411804086497));
#36695=CARTESIAN_POINT('Ctrl Pts',(-25.749961845605,25.9072465457364,-10.3544182485395));
#36696=CARTESIAN_POINT('Ctrl Pts',(-25.6835959627367,25.9674802999819,-10.3603663577646));
#36697=CARTESIAN_POINT('Ctrl Pts',(-25.6134363757629,26.0260136571732,-10.3662814487804));
#36698=CARTESIAN_POINT('Ctrl Pts',(-25.6120699421875,26.0271517405184,-10.3663965121296));
#36699=CARTESIAN_POINT('Ctrl Pts',(-25.6090070836841,26.0296984615862,-10.3666541130383));
#36700=CARTESIAN_POINT('Ctrl Pts',(-25.6073101519687,26.0311064918299,-10.366796618075));
#36701=CARTESIAN_POINT('Ctrl Pts',(-25.6028073070069,26.0348349340807,-10.367174185893));
#36702=CARTESIAN_POINT('Ctrl Pts',(-25.5999988958438,26.0371523412579,-10.3674090856819));
#36703=CARTESIAN_POINT('Ctrl Pts',(-25.5658462902489,26.0652367781078,-10.3702584681927));
#36704=CARTESIAN_POINT('Ctrl Pts',(-25.5340202497699,26.0904159087824,-10.3728403131384));
#36705=CARTESIAN_POINT('Ctrl Pts',(-25.4975235686233,26.1181857371555,-10.3757112434972));
#36706=CARTESIAN_POINT('Ctrl Pts',(-25.4933138863965,26.121372523406,-10.3760410625589));
#36707=CARTESIAN_POINT('Ctrl Pts',(-25.4871152557348,26.1260410520835,-10.3765247419013));
#36708=CARTESIAN_POINT('Ctrl Pts',(-25.4851324256313,26.1275308460571,-10.3766791670963));
#36709=CARTESIAN_POINT('Ctrl Pts',(-25.4816347628029,26.1301524940222,-10.3769510466832));
#36710=CARTESIAN_POINT('Ctrl Pts',(-25.4801206522641,26.1312853047417,-10.3770685689229));
#36711=CARTESIAN_POINT('Ctrl Pts',(-25.4769727259063,26.13363616729,-10.3773125458114));
#36712=CARTESIAN_POINT('Ctrl Pts',(-25.4753387546854,26.1348539999197,-10.3774389849033));
#36713=CARTESIAN_POINT('Ctrl Pts',(-25.4711012710935,26.1380060366129,-10.3777663722579));
#36714=CARTESIAN_POINT('Ctrl Pts',(-25.4684959838848,26.1399378678344,-10.3779671530195));
#36715=CARTESIAN_POINT('Ctrl Pts',(-25.4574481158722,26.1481040883759,-10.3788164663138));
#36716=CARTESIAN_POINT('Ctrl Pts',(-25.4489779002112,26.1543012426461,-10.3794624134995));
#36717=CARTESIAN_POINT('Ctrl Pts',(-25.2999487995973,26.2622232533784,-10.3907394740924));
#36718=CARTESIAN_POINT('Ctrl Pts',(-25.1514079213656,26.3524913545503,-10.4006187100444));
#36719=CARTESIAN_POINT('Ctrl Pts',(-24.780799301934,26.5385663304335,-10.4239075562659));
#36720=CARTESIAN_POINT('Ctrl Pts',(-24.5538531419888,26.6222297956865,-10.4371691245691));
#36721=CARTESIAN_POINT('Ctrl Pts',(-24.2962005002622,26.6855778593387,-10.4526788413348));
#36722=CARTESIAN_POINT('Ctrl Pts',(-24.2726348731474,26.6910911127933,-10.4541006896964));
#36723=CARTESIAN_POINT('Ctrl Pts',(-24.242551413933,26.6977727601466,-10.4559210691844));
#36724=CARTESIAN_POINT('Ctrl Pts',(-24.2360886580852,26.6991872940708,-10.4563124449478));
#36725=CARTESIAN_POINT('Ctrl Pts',(-24.2256234156549,26.7014441254717,-10.4569467304876));
#36726=CARTESIAN_POINT('Ctrl Pts',(-24.2216235811078,26.7022987251038,-10.457189279381));
#36727=CARTESIAN_POINT('Ctrl Pts',(-24.2143451124789,26.703839350972,-10.4576308756856));
#36728=CARTESIAN_POINT('Ctrl Pts',(-24.2110670109104,26.7045278853237,-10.4578298488174));
#36729=CARTESIAN_POINT('Ctrl Pts',(-24.1560273364177,26.7159988846331,-10.4611720969003));
#36730=CARTESIAN_POINT('Ctrl Pts',(-24.1040116901775,26.7255105338787,-10.4643526991278));
#36731=CARTESIAN_POINT('Ctrl Pts',(-24.0431651257261,26.7350964734748,-10.4681064801058));
#36732=CARTESIAN_POINT('Ctrl Pts',(-24.0345370083894,26.7364198691269,-10.4686395390466));
#36733=CARTESIAN_POINT('Ctrl Pts',(-24.0216632658515,26.73834096582,-10.4694360791374));
#36734=CARTESIAN_POINT('Ctrl Pts',(-24.0174216022654,26.738965281897,-10.469698715282));
#36735=CARTESIAN_POINT('Ctrl Pts',(-24.0098511282861,26.7400641246684,-10.4701678101567));
#36736=CARTESIAN_POINT('Ctrl Pts',(-24.006522791117,26.7405419102447,-10.4703741652009));
#36737=CARTESIAN_POINT('Ctrl Pts',(-23.9995755093569,26.7415281041753,-10.4708051432333));
#36738=CARTESIAN_POINT('Ctrl Pts',(-23.9959564373302,26.7420355672553,-10.4710297958756));
#36739=CARTESIAN_POINT('Ctrl Pts',(-23.986470531573,26.7433492243799,-10.4716190054387));
#36740=CARTESIAN_POINT('Ctrl Pts',(-23.9806023449593,26.7441454024292,-10.4719838791925));
#36741=CARTESIAN_POINT('Ctrl Pts',(-23.9677795161654,26.7458491849888,-10.4727820148168));
#36742=CARTESIAN_POINT('Ctrl Pts',(-23.9608240514467,26.7467502681596,-10.4732154816285));
#36743=CARTESIAN_POINT('Ctrl Pts',(-23.9404519885845,26.7493218873508,-10.4744866697063));
#36744=CARTESIAN_POINT('Ctrl Pts',(-23.9270278780822,26.7509306923079,-10.4753263390749));
#36745=CARTESIAN_POINT('Ctrl Pts',(-23.7889539270268,26.7665974159093,-10.4839841655148));
#36746=CARTESIAN_POINT('Ctrl Pts',(-23.6636100162066,26.773449074996,-10.4920293276984));
#36747=CARTESIAN_POINT('Ctrl Pts',(-23.2541100671017,26.771917391328,-10.5189258715085));
#36748=CARTESIAN_POINT('Ctrl Pts',(-22.9714529131186,26.7332992108208,-10.5385757582083));
#36749=CARTESIAN_POINT('Ctrl Pts',(-22.6146964474554,26.6354156880464,-10.5630026097525));
#36750=CARTESIAN_POINT('Ctrl Pts',(-22.5327877612221,26.6093807480631,-10.5685711418652));
#36751=CARTESIAN_POINT('Ctrl Pts',(-22.4460429320873,26.5779379513891,-10.574354953665));
#36752=CARTESIAN_POINT('Ctrl Pts',(-22.4400826561104,26.575757562176,-10.5747517737126));
#36753=CARTESIAN_POINT('Ctrl Pts',(-22.4318148335707,26.572705304213,-10.5753013677805));
#36754=CARTESIAN_POINT('Ctrl Pts',(-22.4295018392485,26.5718483902055,-10.5754550281635));
#36755=CARTESIAN_POINT('Ctrl Pts',(-22.4255242221584,26.5703695741141,-10.5757191119432));
#36756=CARTESIAN_POINT('Ctrl Pts',(-22.4238591303581,26.5697489509085,-10.5758296121771));
#36757=CARTESIAN_POINT('Ctrl Pts',(-22.4204170534887,26.5684627555401,-10.5760579349384));
#36758=CARTESIAN_POINT('Ctrl Pts',(-22.4186401461027,26.5677969923327,-10.5761757451013));
#36759=CARTESIAN_POINT('Ctrl Pts',(-22.4144636335321,26.566227948588,-10.576452518254));
#36760=CARTESIAN_POINT('Ctrl Pts',(-22.4120645099564,26.5653233706262,-10.5766114028691));
#36761=CARTESIAN_POINT('Ctrl Pts',(-22.4042511253066,26.5623667168061,-10.5771285256818));
#36762=CARTESIAN_POINT('Ctrl Pts',(-22.3988412746458,26.5603028977132,-10.5774860600588));
#36763=CARTESIAN_POINT('Ctrl Pts',(-22.2847648255116,26.5164310086626,-10.5850150796031));
#36764=CARTESIAN_POINT('Ctrl Pts',(-22.1784769288177,26.4687942336566,-10.5918347265396));
#36765=CARTESIAN_POINT('Ctrl Pts',(-22.075035905646,26.4155367180763,-10.5984952470527));
#36766=CARTESIAN_POINT('',(-26.7730018644027,23.5481786398916,-10.4357734492733));
#36767=CARTESIAN_POINT('Ctrl Pts',(-22.0750360250409,26.4155367795477,-10.8457129588805));
#36768=CARTESIAN_POINT('Ctrl Pts',(-22.1186364234956,26.4379848237672,-10.8425789699142));
#36769=CARTESIAN_POINT('Ctrl Pts',(-22.1627450527255,26.459435550147,-10.8394118105694));
#36770=CARTESIAN_POINT('Ctrl Pts',(-22.3068659884537,26.5254999520909,-10.8290756717199));
#36771=CARTESIAN_POINT('Ctrl Pts',(-22.4086571099247,26.5660217169583,-10.8217910895913));
#36772=CARTESIAN_POINT('Ctrl Pts',(-22.7472610985681,26.6812133045392,-10.7977341548963));
#36773=CARTESIAN_POINT('Ctrl Pts',(-22.9906690033895,26.7337392538618,-10.780649362133));
#36774=CARTESIAN_POINT('Ctrl Pts',(-23.2722114397519,26.7611734344379,-10.7624927365297));
#36775=CARTESIAN_POINT('Ctrl Pts',(-23.306776414413,26.7639792649023,-10.7602921210766));
#36776=CARTESIAN_POINT('Ctrl Pts',(-23.3459741781228,26.7665250787828,-10.7578338329385));
#36777=CARTESIAN_POINT('Ctrl Pts',(-23.3505673859086,26.7668135191576,-10.7575463490808));
#36778=CARTESIAN_POINT('Ctrl Pts',(-23.3575236717974,26.7672353962311,-10.757111855883));
#36779=CARTESIAN_POINT('Ctrl Pts',(-23.3598862804473,26.7673760690542,-10.7569644420961));
#36780=CARTESIAN_POINT('Ctrl Pts',(-23.3639972328375,26.7676162961331,-10.7567082151541));
#36781=CARTESIAN_POINT('Ctrl Pts',(-23.3657455025255,26.7677170280482,-10.7565993353797));
#36782=CARTESIAN_POINT('Ctrl Pts',(-23.3694076571209,26.7679250396233,-10.7563714432651));
#36783=CARTESIAN_POINT('Ctrl Pts',(-23.3713215547332,26.7680320366399,-10.7562524474683));
#36784=CARTESIAN_POINT('Ctrl Pts',(-23.3759037720577,26.7682841060366,-10.7559677968425));
#36785=CARTESIAN_POINT('Ctrl Pts',(-23.3785721869316,26.7684275677663,-10.7558022333426));
#36786=CARTESIAN_POINT('Ctrl Pts',(-23.3876383268769,26.768903681518,-10.7552403901871));
#36787=CARTESIAN_POINT('Ctrl Pts',(-23.3940369175444,26.7692205786672,-10.7548449948147));
#36788=CARTESIAN_POINT('Ctrl Pts',(-23.4092588850723,26.7699289684798,-10.7539069769913));
#36789=CARTESIAN_POINT('Ctrl Pts',(-23.4180830636382,26.7703032769285,-10.7533652933066));
#36790=CARTESIAN_POINT('Ctrl Pts',(-23.522475620302,26.7743016043603,-10.7469805105668));
#36791=CARTESIAN_POINT('Ctrl Pts',(-23.6181685134833,26.7737064700194,-10.7413602200678));
#36792=CARTESIAN_POINT('Ctrl Pts',(-23.7934804061028,26.764803614745,-10.7312622507125));
#36793=CARTESIAN_POINT('Ctrl Pts',(-23.873083375536,26.7577873743404,-10.7267525480799));
#36794=CARTESIAN_POINT('Ctrl Pts',(-23.9754114797162,26.7449196264872,-10.7209664070455));
#36795=CARTESIAN_POINT('Ctrl Pts',(-23.9984447124259,26.7417696876728,-10.7196647600313));
#36796=CARTESIAN_POINT('Ctrl Pts',(-24.0413981973451,26.7354213574736,-10.7172359457595));
#36797=CARTESIAN_POINT('Ctrl Pts',(-24.0613263473817,26.7322845980414,-10.7161085233793));
#36798=CARTESIAN_POINT('Ctrl Pts',(-24.098747839914,26.7260337145355,-10.7139885111132));
#36799=CARTESIAN_POINT('Ctrl Pts',(-24.1162474076649,26.7229616303184,-10.7129959172454));
#36800=CARTESIAN_POINT('Ctrl Pts',(-24.2950407083182,26.6900477820063,-10.7028357101551));
#36801=CARTESIAN_POINT('Ctrl Pts',(-24.453849231696,26.648079322576,-10.6936379361411));
#36802=CARTESIAN_POINT('Ctrl Pts',(-24.7021016010934,26.5617516392709,-10.6783386398349));
#36803=CARTESIAN_POINT('Ctrl Pts',(-24.7938894798,26.5250209711235,-10.6724715911893));
#36804=CARTESIAN_POINT('Ctrl Pts',(-24.8923505303703,26.4802658324181,-10.6658884371132));
#36805=CARTESIAN_POINT('Ctrl Pts',(-24.9008452840558,26.4763598767592,-10.6653180783301));
#36806=CARTESIAN_POINT('Ctrl Pts',(-24.9134264794258,26.4705084850461,-10.6644697404444));
#36807=CARTESIAN_POINT('Ctrl Pts',(-24.9175260666033,26.4685912929176,-10.6641927388863));
#36808=CARTESIAN_POINT('Ctrl Pts',(-24.9245343095529,26.4652958448211,-10.663718222566));
#36809=CARTESIAN_POINT('Ctrl Pts',(-24.9274449723851,26.463921851221,-10.6635208558686));
#36810=CARTESIAN_POINT('Ctrl Pts',(-24.9332787603214,26.4611572865424,-10.6631246919534));
#36811=CARTESIAN_POINT('Ctrl Pts',(-24.9362018578121,26.4597666674534,-10.6629258932666));
#36812=CARTESIAN_POINT('Ctrl Pts',(-24.9420750918104,26.4569617065763,-10.6625258603448));
#36813=CARTESIAN_POINT('Ctrl Pts',(-24.9450251792501,26.4555472719393,-10.6623246230632));
#36814=CARTESIAN_POINT('Ctrl Pts',(-24.9544155445809,26.4510274138008,-10.6616830983064));
#36815=CARTESIAN_POINT('Ctrl Pts',(-24.9608476107363,26.4479050652257,-10.6612422206946));
#36816=CARTESIAN_POINT('Ctrl Pts',(-24.9985386008922,26.4294533125468,-10.658650119938));
#36817=CARTESIAN_POINT('Ctrl Pts',(-25.0295568576001,26.413640076657,-10.6564819985231));
#36818=CARTESIAN_POINT('Ctrl Pts',(-25.1188597197917,26.3662747614309,-10.6501349854303));
#36819=CARTESIAN_POINT('Ctrl Pts',(-25.1764319868637,26.3334250120501,-10.6459107400589));
#36820=CARTESIAN_POINT('Ctrl Pts',(-25.2934901246181,26.2617612341691,-10.6370394978176));
#36821=CARTESIAN_POINT('Ctrl Pts',(-25.3527879726953,26.2227086367218,-10.632386173533));
#36822=CARTESIAN_POINT('Ctrl Pts',(-25.6656754720295,26.0014928519467,-10.6069852620368));
#36823=CARTESIAN_POINT('Ctrl Pts',(-25.8930407898517,25.7851847057837,-10.5852195151103));
#36824=CARTESIAN_POINT('Ctrl Pts',(-26.0890263970071,25.5353905786491,-10.5648825610526));
#36825=CARTESIAN_POINT('Ctrl Pts',(-26.0922964742507,25.5312013951432,-10.5645427587257));
#36826=CARTESIAN_POINT('Ctrl Pts',(-26.0985817249438,25.5231083844709,-10.5638887549967));
#36827=CARTESIAN_POINT('Ctrl Pts',(-26.1015983258644,25.5192056881396,-10.5635744689783));
#36828=CARTESIAN_POINT('Ctrl Pts',(-26.1099636351831,25.5083316507855,-10.5627018519501));
#36829=CARTESIAN_POINT('Ctrl Pts',(-26.1152928585734,25.5013452756132,-10.5621447123836));
#36830=CARTESIAN_POINT('Ctrl Pts',(-26.1293971596473,25.4826974947723,-10.5606670972836));
#36831=CARTESIAN_POINT('Ctrl Pts',(-26.1381218446569,25.4709979561346,-10.5597498465658));
#36832=CARTESIAN_POINT('Ctrl Pts',(-26.1490105679224,25.4561876245415,-10.5586014133792));
#36833=CARTESIAN_POINT('Ctrl Pts',(-26.1512488204985,25.4531319853079,-10.5583651468825));
#36834=CARTESIAN_POINT('Ctrl Pts',(-26.1547681522083,25.4483096191727,-10.5579933480443));
#36835=CARTESIAN_POINT('Ctrl Pts',(-26.1560528237101,25.4465455372783,-10.557857565181));
#36836=CARTESIAN_POINT('Ctrl Pts',(-26.15842118067,25.443286411606,-10.5576071262134));
#36837=CARTESIAN_POINT('Ctrl Pts',(-26.159505366674,25.4417917502084,-10.557492435334));
#36838=CARTESIAN_POINT('Ctrl Pts',(-26.1619209631023,25.4384555744418,-10.5572367998868));
#36839=CARTESIAN_POINT('Ctrl Pts',(-26.163251707542,25.4366135876298,-10.5570959022119));
#36840=CARTESIAN_POINT('Ctrl Pts',(-26.1670993885261,25.4312758291826,-10.5566883094799));
#36841=CARTESIAN_POINT('Ctrl Pts',(-26.1696112784083,25.4277763995399,-10.5564219653913));
#36842=CARTESIAN_POINT('Ctrl Pts',(-26.1867681528064,25.4037729205623,-10.5546009379943));
#36843=CARTESIAN_POINT('Ctrl Pts',(-26.2011797800713,25.3831020265392,-10.553062140381));
#36844=CARTESIAN_POINT('Ctrl Pts',(-26.2448215143331,25.3189140094615,-10.548366544238));
#36845=CARTESIAN_POINT('Ctrl Pts',(-26.2732348019774,25.2748491961707,-10.5452583038612));
#36846=CARTESIAN_POINT('Ctrl Pts',(-26.4619042194894,24.9659540271525,-10.5241108139773));
#36847=CARTESIAN_POINT('Ctrl Pts',(-26.5843616713091,24.6799193791891,-10.507565278112));
#36848=CARTESIAN_POINT('Ctrl Pts',(-26.669002553184,24.3625769289211,-10.4886402584093));
#36849=CARTESIAN_POINT('Ctrl Pts',(-26.6736987403518,24.3443283387611,-10.4875507373793));
#36850=CARTESIAN_POINT('Ctrl Pts',(-26.6842475491618,24.3017954376839,-10.4850073101816));
#36851=CARTESIAN_POINT('Ctrl Pts',(-26.6899783460662,24.2774823962192,-10.4835503734112));
#36852=CARTESIAN_POINT('Ctrl Pts',(-26.6991928383443,24.2362487785721,-10.4810726185537));
#36853=CARTESIAN_POINT('Ctrl Pts',(-26.7028242113375,24.2193621600604,-10.4800559565639));
#36854=CARTESIAN_POINT('Ctrl Pts',(-26.7073655540932,24.1973859325922,-10.4787299657776));
#36855=CARTESIAN_POINT('Ctrl Pts',(-26.708399310886,24.1923219947657,-10.4784242205001));
#36856=CARTESIAN_POINT('Ctrl Pts',(-26.7102151843335,24.1833163084684,-10.4778801154029));
#36857=CARTESIAN_POINT('Ctrl Pts',(-26.7110021197231,24.1793755348572,-10.4776418965239));
#36858=CARTESIAN_POINT('Ctrl Pts',(-26.7126666403108,24.170958081026,-10.4771327880346));
#36859=CARTESIAN_POINT('Ctrl Pts',(-26.71354209437,24.1664809923417,-10.4768618365091));
#36860=CARTESIAN_POINT('Ctrl Pts',(-26.7157368383524,24.1551291060743,-10.4761743914436));
#36861=CARTESIAN_POINT('Ctrl Pts',(-26.7170432357442,24.1482518641046,-10.4757575181272));
#36862=CARTESIAN_POINT('Ctrl Pts',(-26.7186244927516,24.1397771756368,-10.4752432958245));
#36863=CARTESIAN_POINT('Ctrl Pts',(-26.7189205745393,24.138183670237,-10.4751465835001));
#36864=CARTESIAN_POINT('Ctrl Pts',(-26.7214629390903,24.1244430171188,-10.4743124459254));
#36865=CARTESIAN_POINT('Ctrl Pts',(-26.7236405419754,24.112283395142,-10.4735729655562));
#36866=CARTESIAN_POINT('Ctrl Pts',(-26.7278395703761,24.0880335551028,-10.4720954160416));
#36867=CARTESIAN_POINT('Ctrl Pts',(-26.7298620325906,24.0759437272445,-10.4713573922601));
#36868=CARTESIAN_POINT('Ctrl Pts',(-26.7354777387432,24.0411558345171,-10.469229545288));
#36869=CARTESIAN_POINT('Ctrl Pts',(-26.738897181758,24.0184308369839,-10.4678343817444));
#36870=CARTESIAN_POINT('Ctrl Pts',(-26.74296793344,23.9892603127437,-10.4660362987347));
#36871=CARTESIAN_POINT('Ctrl Pts',(-26.7438433132651,23.9828463218323,-10.4656404926972));
#36872=CARTESIAN_POINT('Ctrl Pts',(-26.7452077396333,23.9726191509497,-10.465008652282));
#36873=CARTESIAN_POINT('Ctrl Pts',(-26.7457093014396,23.9688076347377,-10.4647730145555));
#36874=CARTESIAN_POINT('Ctrl Pts',(-26.7466327308141,23.9616918122765,-10.4643327939177));
#36875=CARTESIAN_POINT('Ctrl Pts',(-26.7470562979422,23.9583877285369,-10.4641282651092));
#36876=CARTESIAN_POINT('Ctrl Pts',(-26.7478779461743,23.9518986123362,-10.4637263360939));
#36877=CARTESIAN_POINT('Ctrl Pts',(-26.748276393221,23.9487136294325,-10.4635289477265));
#36878=CARTESIAN_POINT('Ctrl Pts',(-26.7491615030231,23.9415516614389,-10.4630848286318));
#36879=CARTESIAN_POINT('Ctrl Pts',(-26.7496455081749,23.937574358605,-10.4628380140951));
#36880=CARTESIAN_POINT('Ctrl Pts',(-26.7508429064305,23.9275793625489,-10.4622173127949));
#36881=CARTESIAN_POINT('Ctrl Pts',(-26.7515467437073,23.9215605594346,-10.4618431243511));
#36882=CARTESIAN_POINT('Ctrl Pts',(-26.752860338551,23.9100460454496,-10.4611264656767));
#36883=CARTESIAN_POINT('Ctrl Pts',(-26.7534729365567,23.9045506749863,-10.4607840868392));
#36884=CARTESIAN_POINT('Ctrl Pts',(-26.7667647450157,23.7824623899342,-10.4531697521634));
#36885=CARTESIAN_POINT('Ctrl Pts',(-26.7730826164252,23.665281353586,-10.4456974470109));
#36886=CARTESIAN_POINT('Ctrl Pts',(-26.773001765511,23.5480302730957,-10.4380474642037));
#36887=CARTESIAN_POINT('Ctrl Pts',(-26.7730018644027,23.5481786398916,-10.4357734492733));
#36888=CARTESIAN_POINT('Ctrl Pts',(-26.7729292341586,23.4353139908667,-10.4288341238586));
#36889=CARTESIAN_POINT('Ctrl Pts',(-26.7669235627087,23.3226754865815,-10.421894798444));
#36890=CARTESIAN_POINT('Ctrl Pts',(-26.755080179162,23.2108452357707,-10.4149554730293));
#36891=CARTESIAN_POINT('Ctrl Pts',(-26.7431850598284,23.0985264737172,-10.4079858343635));
#36892=CARTESIAN_POINT('Ctrl Pts',(-26.7254012379132,22.9870232448594,-10.4010161956977));
#36893=CARTESIAN_POINT('Ctrl Pts',(-26.7018749653354,22.8769074505733,-10.3940465570318));
#36894=CARTESIAN_POINT('Ctrl Pts',(-26.6782170628028,22.7661755562667,-10.3870379231015));
#36895=CARTESIAN_POINT('Ctrl Pts',(-26.6487523832634,22.6568468639344,-10.3800292891711));
#36896=CARTESIAN_POINT('Ctrl Pts',(-26.6136780058931,22.5494818653927,-10.3730206552408));
#36897=CARTESIAN_POINT('Ctrl Pts',(-26.5948831962548,22.4919497048615,-10.3692650378807));
#36898=CARTESIAN_POINT('Ctrl Pts',(-26.5744784225793,22.4349810255353,-10.3655094205207));
#36899=CARTESIAN_POINT('Ctrl Pts',(-26.5524995027409,22.3786593056378,-10.3617538031606));
#36900=CARTESIAN_POINT('Ctrl Pts',(-26.5163787036329,22.2860985453826,-10.3555817118483));
#36901=CARTESIAN_POINT('Ctrl Pts',(-26.4759097362695,22.1950467644762,-10.349409620536));
#36902=CARTESIAN_POINT('Ctrl Pts',(-26.4312391033891,22.1059416454188,-10.3432375292236));
#36903=CARTESIAN_POINT('Ctrl Pts',(-26.3866289948,22.0169572549884,-10.3370738004848));
#36904=CARTESIAN_POINT('Ctrl Pts',(-26.3378287287879,21.9299146689386,-10.330910071746));
#36905=CARTESIAN_POINT('Ctrl Pts',(-26.2850334753614,21.8452332494998,-10.3247463430072));
#36906=CARTESIAN_POINT('Ctrl Pts',(-26.2322941535509,21.7606415420773,-10.3185891441606));
#36907=CARTESIAN_POINT('Ctrl Pts',(-26.1755684871054,21.6784063947794,-10.3124319453139));
#36908=CARTESIAN_POINT('Ctrl Pts',(-26.1150978754791,21.5989232604114,-10.3062747464672));
#36909=CARTESIAN_POINT('Ctrl Pts',(-26.0546714642027,21.5194982233945,-10.3001220481595));
#36910=CARTESIAN_POINT('Ctrl Pts',(-25.990505812244,21.4428215446761,-10.2939693498518));
#36911=CARTESIAN_POINT('Ctrl Pts',(-25.9228854899555,21.3692595450314,-10.2878166515441));
#36912=CARTESIAN_POINT('Ctrl Pts',(-25.8552908093894,21.2957254402017,-10.2816662863483));
#36913=CARTESIAN_POINT('Ctrl Pts',(-25.7842443551357,21.2253039870875,-10.2755159211526));
#36914=CARTESIAN_POINT('Ctrl Pts',(-25.7100702408391,21.1583275692917,-10.2693655559568));
#36915=CARTESIAN_POINT('Ctrl Pts',(-25.6359044097136,21.091358630886,-10.2632158775846));
#36916=CARTESIAN_POINT('Ctrl Pts',(-25.5586119353587,21.0278342540622,-10.2570661992124));
#36917=CARTESIAN_POINT('Ctrl Pts',(-25.4785522209244,20.9680484593918,-10.2509165208402));
#36918=CARTESIAN_POINT('Ctrl Pts',(-25.3984800287558,20.908253346786,-10.2447658840077));
#36919=CARTESIAN_POINT('Ctrl Pts',(-25.3156400879515,20.8521982336258,-10.2386152471753));
#36920=CARTESIAN_POINT('Ctrl Pts',(-25.2304223334371,20.8001348978808,-10.2324646103428));
#36921=CARTESIAN_POINT('Ctrl Pts',(-25.1451134138266,20.7480158653033,-10.226307393621));
#36922=CARTESIAN_POINT('Ctrl Pts',(-25.0574219722847,20.6998973645516,-10.2201501768992));
#36923=CARTESIAN_POINT('Ctrl Pts',(-24.9677640970661,20.6559860400703,-10.2139929601774));
#36924=CARTESIAN_POINT('Ctrl Pts',(-24.8780562020862,20.612050217641,-10.2078323083696));
#36925=CARTESIAN_POINT('Ctrl Pts',(-24.7863800872479,20.5723264185468,-10.2016716565618));
#36926=CARTESIAN_POINT('Ctrl Pts',(-24.6931715070611,20.5369729598247,-10.195511004754));
#36927=CARTESIAN_POINT('Ctrl Pts',(-24.5998069557743,20.5015603421942,-10.1893400439849));
#36928=CARTESIAN_POINT('Ctrl Pts',(-24.5049052299846,20.4705328078024,-10.1831690832159));
#36929=CARTESIAN_POINT('Ctrl Pts',(-24.4089170475075,20.4439987088743,-10.1769981224469));
#36930=CARTESIAN_POINT('Ctrl Pts',(-24.3356474655575,20.4237447329607,-10.1722877122265));
#36931=CARTESIAN_POINT('Ctrl Pts',(-24.2617451641514,20.4061078490576,-10.1675773020061));
#36932=CARTESIAN_POINT('Ctrl Pts',(-24.187413255466,20.3911159764655,-10.1628668917857));
#36933=CARTESIAN_POINT('Ctrl Pts',(-24.0900155116688,20.3714719959516,-10.1566948004734));
#36934=CARTESIAN_POINT('Ctrl Pts',(-23.9915369282417,20.3563018696539,-10.1505227091611));
#36935=CARTESIAN_POINT('Ctrl Pts',(-23.8924249257566,20.3457189283064,-10.1443506178487));
#36936=CARTESIAN_POINT('Ctrl Pts',(-23.7934472102364,20.3351503257982,-10.1381868891099));
#36937=CARTESIAN_POINT('Ctrl Pts',(-23.6938382096012,20.32915660062,-10.1320231603712));
#36938=CARTESIAN_POINT('Ctrl Pts',(-23.594056237995,20.3278002360327,-10.1258594316324));
#36939=CARTESIAN_POINT('Ctrl Pts',(-23.4943799760226,20.3264453083863,-10.1197022327857));
#36940=CARTESIAN_POINT('Ctrl Pts',(-23.3945315393536,20.3297179800143,-10.113545033939));
#36941=CARTESIAN_POINT('Ctrl Pts',(-23.2949741157067,20.3376289165113,-10.1073878350923));
#36942=CARTESIAN_POINT('Ctrl Pts',(-23.1954894624993,20.3455340705934,-10.1012351367846));
#36943=CARTESIAN_POINT('Ctrl Pts',(-23.0962958311345,20.358070714771,-10.0950824384769));
#36944=CARTESIAN_POINT('Ctrl Pts',(-22.9978552357661,20.3751974471403,-10.0889297401692));
#36945=CARTESIAN_POINT('Ctrl Pts',(-22.8994519692116,20.3923176850284,-10.0827793749734));
#36946=CARTESIAN_POINT('Ctrl Pts',(-22.801801598761,20.4140244782415,-10.0766290097777));
#36947=CARTESIAN_POINT('Ctrl Pts',(-22.7053589614813,20.4402248119604,-10.0704786445819));
#36948=CARTESIAN_POINT('Ctrl Pts',(-22.6089270941431,20.4664222198357,-10.0643289662097));
#36949=CARTESIAN_POINT('Ctrl Pts',(-22.5137031110442,20.49711205668,-10.0581792878375));
#36950=CARTESIAN_POINT('Ctrl Pts',(-22.4201286492632,20.5321508811763,-10.0520296094653));
#36951=CARTESIAN_POINT('Ctrl Pts',(-22.3265396034023,20.5671951666606,-10.0458789726328));
#36952=CARTESIAN_POINT('Ctrl Pts',(-22.2346009963549,20.6065896337603,-10.0397283358004));
#36953=CARTESIAN_POINT('Ctrl Pts',(-22.1447354295089,20.6501423203463,-10.0335776989679));
#36954=CARTESIAN_POINT('Ctrl Pts',(-22.0547737253841,20.6937415991579,-10.0274204822461));
#36955=CARTESIAN_POINT('Ctrl Pts',(-21.9668898817002,20.7415077906915,-10.0212632655243));
#36956=CARTESIAN_POINT('Ctrl Pts',(-21.8814826652363,20.7932025329996,-10.0151060488025));
#36957=CARTESIAN_POINT('Ctrl Pts',(-21.7960278004361,20.8449261155927,-10.0089453969947));
#36958=CARTESIAN_POINT('Ctrl Pts',(-21.713052675266,20.900582371749,-10.0027847451869));
#36959=CARTESIAN_POINT('Ctrl Pts',(-21.6329260282908,20.9598902709579,-9.99662409337905));
#36960=CARTESIAN_POINT('Ctrl Pts',(-21.5526653009419,21.0192974133723,-9.99045313261002));
#36961=CARTESIAN_POINT('Ctrl Pts',(-21.4752629097114,21.0823681298745,-9.98428217184101));
#36962=CARTESIAN_POINT('Ctrl Pts',(-21.4010536452309,21.1487817929749,-9.97811121107198));
#36963=CARTESIAN_POINT('Ctrl Pts',(-21.3444083203067,21.1994765889962,-9.9734008008516));
#36964=CARTESIAN_POINT('Ctrl Pts',(-21.2896227871122,21.2521183516899,-9.96869039063121));
#36965=CARTESIAN_POINT('Ctrl Pts',(-21.2368303253655,21.3065512909393,-9.96397998041083));
#36966=CARTESIAN_POINT('Ctrl Pts',(-21.1676559054618,21.3778752427241,-9.9578078890985));
#36967=CARTESIAN_POINT('Ctrl Pts',(-21.1016611745336,21.4525268308881,-9.95163579778617));
#36968=CARTESIAN_POINT('Ctrl Pts',(-21.0391833294155,21.5301908930634,-9.94546370647384));
#36969=CARTESIAN_POINT('Ctrl Pts',(-20.9767901356009,21.6077497281126,-9.93929997773506));
#36970=CARTESIAN_POINT('Ctrl Pts',(-20.9179046264757,21.6883125890606,-9.93313624899627));
#36971=CARTESIAN_POINT('Ctrl Pts',(-20.8628271084798,21.7715276633796,-9.92697252025748));
#36972=CARTESIAN_POINT('Ctrl Pts',(-20.8078079399448,21.8546545791375,-9.9208153214108));
#36973=CARTESIAN_POINT('Ctrl Pts',(-20.7565889806,21.9404277619421,-9.91465812256414));
#36974=CARTESIAN_POINT('Ctrl Pts',(-20.7094295761867,22.0284632894002,-9.90850092371745));
#36975=CARTESIAN_POINT('Ctrl Pts',(-20.6623046424382,22.1164344682264,-9.90234822540975));
#36976=CARTESIAN_POINT('Ctrl Pts',(-20.6192335686585,22.2066643222329,-9.896195527102));
#36977=CARTESIAN_POINT('Ctrl Pts',(-20.5804312609677,22.2987417716763,-9.89004282879429));
#36978=CARTESIAN_POINT('Ctrl Pts',(-20.5416436671672,22.3907843052198,-9.88389246359854));
#36979=CARTESIAN_POINT('Ctrl Pts',(-20.5071217915778,22.4846726422299,-9.87774209840284));
#36980=CARTESIAN_POINT('Ctrl Pts',(-20.4770332379878,22.5799738421977,-9.87159173320708));
#36981=CARTESIAN_POINT('Ctrl Pts',(-20.4469480444467,22.6752643996906,-9.86544205483487));
#36982=CARTESIAN_POINT('Ctrl Pts',(-20.4212953194093,22.7719670922121,-9.85929237646264));
#36983=CARTESIAN_POINT('Ctrl Pts',(-20.4001931068524,22.8696328269653,-9.85314269809042));
#36984=CARTESIAN_POINT('Ctrl Pts',(-20.3790876054029,22.9673137834452,-9.84699206125797));
#36985=CARTESIAN_POINT('Ctrl Pts',(-20.3625341168807,23.0659576556402,-9.84084142442551));
#36986=CARTESIAN_POINT('Ctrl Pts',(-20.3505995742911,23.1651051382437,-9.83469078759306));
#36987=CARTESIAN_POINT('Ctrl Pts',(-20.3386522642481,23.2643586878258,-9.82853357087125));
#36988=CARTESIAN_POINT('Ctrl Pts',(-20.3313338194465,23.3641164915305,-9.82237635414945));
#36989=CARTESIAN_POINT('Ctrl Pts',(-20.3286592523298,23.4639142154381,-9.81621913742764));
#36990=CARTESIAN_POINT('Ctrl Pts',(-20.325983193083,23.5637676160871,-9.81005848561984));
#36991=CARTESIAN_POINT('Ctrl Pts',(-20.327956162482,23.6636605469585,-9.80389783381202));
#36992=CARTESIAN_POINT('Ctrl Pts',(-20.3345410436693,23.7631308732061,-9.79773718200421));
#36993=CARTESIAN_POINT('Ctrl Pts',(-20.3411369437044,23.8627676486816,-9.79156622123518));
#36994=CARTESIAN_POINT('Ctrl Pts',(-20.3523601219335,23.9619799751271,-9.78539526046612));
#36995=CARTESIAN_POINT('Ctrl Pts',(-20.3681217975989,24.0603128748168,-9.77922429969709));
#36996=CARTESIAN_POINT('Ctrl Pts',(-20.3801529805741,24.1353722234393,-9.7745138894767));
#36997=CARTESIAN_POINT('Ctrl Pts',(-20.3948274755497,24.2099193160998,-9.76980347925633));
#36998=CARTESIAN_POINT('Ctrl Pts',(-20.4120862570241,24.2837578111728,-9.76509306903594));
#36999=CARTESIAN_POINT('Ctrl Pts',(-20.4347027313341,24.3805182012034,-9.75892039271475));
#37000=CARTESIAN_POINT('Ctrl Pts',(-20.4618384160323,24.4764020278299,-9.75274771639359));
#37001=CARTESIAN_POINT('Ctrl Pts',(-20.4934104028952,24.5709551142811,-9.7465750400724));
#37002=CARTESIAN_POINT('Ctrl Pts',(-20.5261462377295,24.6689937405667,-9.74017481846411));
#37003=CARTESIAN_POINT('Ctrl Pts',(-20.5636517547069,24.7656011521383,-9.73377459685581));
#37004=CARTESIAN_POINT('Ctrl Pts',(-20.6057762256289,24.860281861717,-9.72737437524752));
#37005=CARTESIAN_POINT('Ctrl Pts',(-20.6462960525434,24.9513559068099,-9.72121795675476));
#37006=CARTESIAN_POINT('Ctrl Pts',(-20.6910891794856,25.0406469057963,-9.71506153826197));
#37007=CARTESIAN_POINT('Ctrl Pts',(-20.7399709965839,25.1277300294476,-9.70890511976921));
#37008=CARTESIAN_POINT('Ctrl Pts',(-20.7888200647944,25.2147548108437,-9.70275282583381));
#37009=CARTESIAN_POINT('Ctrl Pts',(-20.8417521675508,25.2995742789073,-9.6966005318984));
#37010=CARTESIAN_POINT('Ctrl Pts',(-20.898535909008,25.3817864558872,-9.690448237963));
#37011=CARTESIAN_POINT('Ctrl Pts',(-20.9552967994043,25.463965548829,-9.68429841984973));
#37012=CARTESIAN_POINT('Ctrl Pts',(-21.0159060003052,25.5435390798167,-9.67814860173648));
#37013=CARTESIAN_POINT('Ctrl Pts',(-21.0800883176759,25.6201332814678,-9.67199878362321));
#37014=CARTESIAN_POINT('Ctrl Pts',(-21.1442619770477,25.6967171507946,-9.66584979510166));
#37015=CARTESIAN_POINT('Ctrl Pts',(-21.2120075140709,25.7703221584116,-9.6597008065801));
#37016=CARTESIAN_POINT('Ctrl Pts',(-21.2830095503844,25.8406077063781,-9.65355181805855));
#37017=CARTESIAN_POINT('Ctrl Pts',(-21.3540485173879,25.9109298123634,-9.64739963122888));
#37018=CARTESIAN_POINT('Ctrl Pts',(-21.4283470578706,25.9779287042374,-9.64124744439921));
#37019=CARTESIAN_POINT('Ctrl Pts',(-21.5055533802708,26.0413010945826,-9.63509525756955));
#37020=CARTESIAN_POINT('Ctrl Pts',(-21.5827839279436,26.1046933694837,-9.62894114034871));
#37021=CARTESIAN_POINT('Ctrl Pts',(-21.662923729402,26.1644566129475,-9.6227870231279));
#37022=CARTESIAN_POINT('Ctrl Pts',(-21.7455897448107,26.2203292699431,-9.61663290590707));
#37023=CARTESIAN_POINT('Ctrl Pts',(-21.8283399051361,26.2762587991618,-9.61047252447139));
#37024=CARTESIAN_POINT('Ctrl Pts',(-21.913621043207,26.3282896083141,-9.60431214303569));
#37025=CARTESIAN_POINT('Ctrl Pts',(-22.0010234910573,26.3762049272853,-9.59815176160001));
#37026=CARTESIAN_POINT('Ctrl Pts',(-22.0255307934407,26.3896401941424,-9.59642441489114));
#37027=CARTESIAN_POINT('Ctrl Pts',(-22.0502047432709,26.4027521781315,-9.59469706818227));
#37028=CARTESIAN_POINT('Ctrl Pts',(-22.0750360153461,26.4155367745563,-9.59296972147339));
#37029=CARTESIAN_POINT('Origin',(-23.5502525316942,23.5502525316942,-77.3107734492734));
#37030=CARTESIAN_POINT('',(-22.0750359919087,26.4155367624894,-8.09328852648195));
#37031=CARTESIAN_POINT('',(-22.0750360458934,26.4155367902838,-8.34120882940695));
#37032=CARTESIAN_POINT('',(-22.0750360153461,26.4155367745563,-77.3107734492734));
#37033=CARTESIAN_POINT('',(-26.773001214148,23.5531666769314,-8.93957441054318));
#37034=CARTESIAN_POINT('Ctrl Pts',(-22.0750359919087,26.4155367624894,-8.09328852648195));
#37035=CARTESIAN_POINT('Ctrl Pts',(-21.9573065708424,26.354922744756,-8.10161611668175));
#37036=CARTESIAN_POINT('Ctrl Pts',(-21.8434252301781,26.2871108196349,-8.11019806025512));
#37037=CARTESIAN_POINT('Ctrl Pts',(-21.5403771928706,26.0803666436431,-8.13450590777129));
#37038=CARTESIAN_POINT('Ctrl Pts',(-21.3617299474878,25.927526736386,-8.15061384987241));
#37039=CARTESIAN_POINT('Ctrl Pts',(-21.1273775541537,25.678029700849,-8.1734080311854));
#37040=CARTESIAN_POINT('Ctrl Pts',(-21.0574951103024,25.5957170105429,-8.18046132516641));
#37041=CARTESIAN_POINT('Ctrl Pts',(-20.9878143459113,25.5047531131256,-8.18764675290268));
#37042=CARTESIAN_POINT('Ctrl Pts',(-20.9837779343401,25.4994498335995,-8.18806356127619));
#37043=CARTESIAN_POINT('Ctrl Pts',(-20.978238786992,25.492125133863,-8.18863629861809));
#37044=CARTESIAN_POINT('Ctrl Pts',(-20.9767219627746,25.4901144641352,-8.18879321376207));
#37045=CARTESIAN_POINT('Ctrl Pts',(-20.9741306040372,25.4866710256537,-8.18906142062471));
#37046=CARTESIAN_POINT('Ctrl Pts',(-20.9730549070567,25.4852391397878,-8.18917279464785));
#37047=CARTESIAN_POINT('Ctrl Pts',(-20.9709600497518,25.4824457796315,-8.18938976372299));
#37048=CARTESIAN_POINT('Ctrl Pts',(-20.9699407763217,25.4810843990186,-8.18949536655215));
#37049=CARTESIAN_POINT('Ctrl Pts',(-20.9674807358536,25.4777932479724,-8.18975032594651));
#37050=CARTESIAN_POINT('Ctrl Pts',(-20.9660410502544,25.4758626639862,-8.18989960572073));
#37051=CARTESIAN_POINT('Ctrl Pts',(-20.9616965984248,25.470023210618,-8.19035029706649));
#37052=CARTESIAN_POINT('Ctrl Pts',(-20.9587985101012,25.4661093462885,-8.19065123989692));
#37053=CARTESIAN_POINT('Ctrl Pts',(-20.9302781950621,25.4274095819416,-8.19361594253352));
#37054=CARTESIAN_POINT('Ctrl Pts',(-20.905347512274,25.392116262991,-8.19623230094382));
#37055=CARTESIAN_POINT('Ctrl Pts',(-20.834113323417,25.2868424997952,-8.20381716082002));
#37056=CARTESIAN_POINT('Ctrl Pts',(-20.7898217525837,25.215539596482,-8.20867762667879));
#37057=CARTESIAN_POINT('Ctrl Pts',(-20.6533529590857,24.9754069385022,-8.22442973516083));
#37058=CARTESIAN_POINT('Ctrl Pts',(-20.5734954248659,24.8000583860983,-8.23499146268696));
#37059=CARTESIAN_POINT('Ctrl Pts',(-20.4473888278571,24.4411705566913,-8.25646728967847));
#37060=CARTESIAN_POINT('Ctrl Pts',(-20.4006973012122,24.2586196390261,-8.2673313588744));
#37061=CARTESIAN_POINT('Ctrl Pts',(-20.3681718124855,24.0607764969554,-8.27951619730709));
#37062=CARTESIAN_POINT('Ctrl Pts',(-20.3662242296477,24.0484855972591,-8.28027469742689));
#37063=CARTESIAN_POINT('Ctrl Pts',(-20.3636550050387,24.0316410266239,-8.28131639530575));
#37064=CARTESIAN_POINT('Ctrl Pts',(-20.3629718279045,24.0270967356345,-8.28159763911032));
#37065=CARTESIAN_POINT('Ctrl Pts',(-20.3618239169232,24.0193484838624,-8.28207754946121));
#37066=CARTESIAN_POINT('Ctrl Pts',(-20.3613542858122,24.0161452458761,-8.2822760604407));
#37067=CARTESIAN_POINT('Ctrl Pts',(-20.3604539345899,24.0099390290277,-8.28266088552741));
#37068=CARTESIAN_POINT('Ctrl Pts',(-20.3600226263091,24.0069361383715,-8.28284718072536));
#37069=CARTESIAN_POINT('Ctrl Pts',(-20.3590071832156,23.9997946956526,-8.28329045818412));
#37070=CARTESIAN_POINT('Ctrl Pts',(-20.3584268590817,23.9956556151497,-8.28354756093572));
#37071=CARTESIAN_POINT('Ctrl Pts',(-20.3567437746367,23.9834790299398,-8.28430447201234));
#37072=CARTESIAN_POINT('Ctrl Pts',(-20.3556633166317,23.9754385207178,-8.28480498596277));
#37073=CARTESIAN_POINT('Ctrl Pts',(-20.3475239854818,23.9130847062843,-8.28869203985816));
#37074=CARTESIAN_POINT('Ctrl Pts',(-20.3418207263208,23.8586063568136,-8.29212123062283));
#37075=CARTESIAN_POINT('Ctrl Pts',(-20.3271819304938,23.6732703987473,-8.30390953093639));
#37076=CARTESIAN_POINT('Ctrl Pts',(-20.3248467159278,23.5420364197295,-8.31246908498272));
#37077=CARTESIAN_POINT('Ctrl Pts',(-20.3383294394444,23.2302087255335,-8.3332499117462));
#37078=CARTESIAN_POINT('Ctrl Pts',(-20.3613681783913,23.0503636642574,-8.34560086238983));
#37079=CARTESIAN_POINT('Ctrl Pts',(-20.4290269267916,22.7353915105678,-8.36726555311397));
#37080=CARTESIAN_POINT('Ctrl Pts',(-20.4677177665171,22.5994435144559,-8.37661941945852));
#37081=CARTESIAN_POINT('Ctrl Pts',(-20.5182674765082,22.4578849084121,-8.38606982996712));
#37082=CARTESIAN_POINT('Ctrl Pts',(-20.5213646003374,22.4493264200469,-8.3866400139683));
#37083=CARTESIAN_POINT('Ctrl Pts',(-20.5255948755178,22.4377895986684,-8.38740691651851));
#37084=CARTESIAN_POINT('Ctrl Pts',(-20.5266962084174,22.4347997650539,-8.38760550880069));
#37085=CARTESIAN_POINT('Ctrl Pts',(-20.5284346180392,22.4301019247316,-8.38791730191848));
#37086=CARTESIAN_POINT('Ctrl Pts',(-20.5290687092669,22.4283928271372,-8.38803068187137));
#37087=CARTESIAN_POINT('Ctrl Pts',(-20.5302931807261,22.4251010154478,-8.38824895624923));
#37088=CARTESIAN_POINT('Ctrl Pts',(-20.5308833512837,22.4235182380774,-8.38835386212594));
#37089=CARTESIAN_POINT('Ctrl Pts',(-20.5322897679984,22.419755411725,-8.38860315382899));
#37090=CARTESIAN_POINT('Ctrl Pts',(-20.5331071311787,22.4175757845403,-8.38874747141705));
#37091=CARTESIAN_POINT('Ctrl Pts',(-20.5355047382168,22.4112031990482,-8.38916916910932));
#37092=CARTESIAN_POINT('Ctrl Pts',(-20.5370913742377,22.4070126267532,-8.38944616531073));
#37093=CARTESIAN_POINT('Ctrl Pts',(-20.5492608158052,22.3750724093487,-8.39155514455531));
#37094=CARTESIAN_POINT('Ctrl Pts',(-20.5602184625373,22.3474657605841,-8.39336493263201));
#37095=CARTESIAN_POINT('Ctrl Pts',(-20.5988637072362,22.2538966127567,-8.39946710842424));
#37096=CARTESIAN_POINT('Ctrl Pts',(-20.6283666745114,22.1887022173879,-8.40366441416358));
#37097=CARTESIAN_POINT('Ctrl Pts',(-20.7354038888723,21.9717141908156,-8.41762300153342));
#37098=CARTESIAN_POINT('Ctrl Pts',(-20.8227972346321,21.8251001143924,-8.42704664337351));
#37099=CARTESIAN_POINT('Ctrl Pts',(-21.0082678604624,21.5635480779807,-8.44499673029432));
#37100=CARTESIAN_POINT('Ctrl Pts',(-21.1036102626014,21.4472506895518,-8.4534747028518));
#37101=CARTESIAN_POINT('Ctrl Pts',(-21.2246285027271,21.319048370053,-8.46377675624882));
#37102=CARTESIAN_POINT('Ctrl Pts',(-21.2427789758806,21.3002825605042,-8.46531059699426));
#37103=CARTESIAN_POINT('Ctrl Pts',(-21.2644155381146,21.2784496669926,-8.46712720679567));
#37104=CARTESIAN_POINT('Ctrl Pts',(-21.2676830592542,21.2751666826622,-8.46740123571817));
#37105=CARTESIAN_POINT('Ctrl Pts',(-21.2737931508909,21.2690540885643,-8.46791308342342));
#37106=CARTESIAN_POINT('Ctrl Pts',(-21.2766339506186,21.2662227164401,-8.46815083037824));
#37107=CARTESIAN_POINT('Ctrl Pts',(-21.2829969721644,21.2599044457422,-8.46868284880503));
#37108=CARTESIAN_POINT('Ctrl Pts',(-21.2865219620928,21.2564203593448,-8.46897723318948));
#37109=CARTESIAN_POINT('Ctrl Pts',(-21.2949976781262,21.2480815593424,-8.46968426381833));
#37110=CARTESIAN_POINT('Ctrl Pts',(-21.2999560479873,21.2432346785305,-8.47009722668026));
#37111=CARTESIAN_POINT('Ctrl Pts',(-21.3063472510161,21.2370273897882,-8.47062870592974));
#37112=CARTESIAN_POINT('Ctrl Pts',(-21.3077657718126,21.2356522211586,-8.4707466156265));
#37113=CARTESIAN_POINT('Ctrl Pts',(-21.3130255933399,21.2305625217665,-8.47118363091039));
#37114=CARTESIAN_POINT('Ctrl Pts',(-21.3168748513546,21.2268562563436,-8.47150307504396));
#37115=CARTESIAN_POINT('Ctrl Pts',(-21.3226728131037,21.2213013998617,-8.47198369030811));
#37116=CARTESIAN_POINT('Ctrl Pts',(-21.3246146518515,21.2194456317378,-8.47214456468561));
#37117=CARTESIAN_POINT('Ctrl Pts',(-21.3323351459601,21.2120857882112,-8.47278381842538));
#37118=CARTESIAN_POINT('Ctrl Pts',(-21.3381318822736,21.2066007911476,-8.47326298323059));
#37119=CARTESIAN_POINT('Ctrl Pts',(-21.3647996812133,21.1815542272336,-8.4754638154192));
#37120=CARTESIAN_POINT('Ctrl Pts',(-21.3859097364079,21.1622500185959,-8.47719605813919));
#37121=CARTESIAN_POINT('Ctrl Pts',(-21.4126077977254,21.1384806594419,-8.47937578269444));
#37122=CARTESIAN_POINT('Ctrl Pts',(-21.4179578802664,21.1337492540945,-8.47981203633124));
#37123=CARTESIAN_POINT('Ctrl Pts',(-21.4265892119216,21.1261670216064,-8.48051499253071));
#37124=CARTESIAN_POINT('Ctrl Pts',(-21.4298605986814,21.1233049619914,-8.48078122566481));
#37125=CARTESIAN_POINT('Ctrl Pts',(-21.4356861102275,21.1182291280112,-8.4812549758304));
#37126=CARTESIAN_POINT('Ctrl Pts',(-21.4382379512898,21.1160127327267,-8.48146238342603));
#37127=CARTESIAN_POINT('Ctrl Pts',(-21.443562457163,21.1114028214842,-8.48189490640814));
#37128=CARTESIAN_POINT('Ctrl Pts',(-21.4463357239177,21.109010010989,-8.48212005061243));
#37129=CARTESIAN_POINT('Ctrl Pts',(-21.4535337327445,21.1028208510722,-8.48270406599189));
#37130=CARTESIAN_POINT('Ctrl Pts',(-21.457964693641,21.09903178374,-8.48306323732909));
#37131=CARTESIAN_POINT('Ctrl Pts',(-21.4764944432798,21.0832732049138,-8.48456386754899));
#37132=CARTESIAN_POINT('Ctrl Pts',(-21.4906856323746,21.0714133331376,-8.48570981834527));
#37133=CARTESIAN_POINT('Ctrl Pts',(-21.5272907129781,21.0413530413518,-8.48865767838952));
#37134=CARTESIAN_POINT('Ctrl Pts',(-21.5498481627544,21.0233307984716,-8.4904666840662));
#37135=CARTESIAN_POINT('Ctrl Pts',(-21.6277837373006,20.9627618506007,-8.49669261457061));
#37136=CARTESIAN_POINT('Ctrl Pts',(-21.6842979353195,20.921715573079,-8.50116691565166));
#37137=CARTESIAN_POINT('Ctrl Pts',(-21.9160538687353,20.7646331999288,-8.51936029325104));
#37138=CARTESIAN_POINT('Ctrl Pts',(-22.1011077055038,20.6640371537043,-8.53358897655656));
#37139=CARTESIAN_POINT('Ctrl Pts',(-22.3192744424469,20.5717414982212,-8.54961281572385));
#37140=CARTESIAN_POINT('Ctrl Pts',(-22.3440726763337,20.5616131744564,-8.55142306099604));
#37141=CARTESIAN_POINT('Ctrl Pts',(-22.515829278821,20.4939487563055,-8.56387478419597));
#37142=CARTESIAN_POINT('Ctrl Pts',(-22.6667360821941,20.4469580885852,-8.57439230469254));
#37143=CARTESIAN_POINT('Ctrl Pts',(-22.8296221596707,20.409090772024,-8.58490909751607));
#37144=CARTESIAN_POINT('Ctrl Pts',(-22.8387567737052,20.4070091231993,-8.5854961181882));
#37145=CARTESIAN_POINT('Ctrl Pts',(-22.8510460918294,20.4042648798913,-8.58628204590355));
#37146=CARTESIAN_POINT('Ctrl Pts',(-22.8541927827349,20.4035671681822,-8.58648294693222));
#37147=CARTESIAN_POINT('Ctrl Pts',(-22.8591280460063,20.4024806438571,-8.58679750654798));
#37148=CARTESIAN_POINT('Ctrl Pts',(-22.8609159009117,20.4020886347414,-8.5869113497083));
#37149=CARTESIAN_POINT('Ctrl Pts',(-22.8643525294807,20.4013381796707,-8.5871299679914));
#37150=CARTESIAN_POINT('Ctrl Pts',(-22.8660012398631,20.4009795077951,-8.58723475546849));
#37151=CARTESIAN_POINT('Ctrl Pts',(-22.8699096467533,20.40013246,-8.58748294142765));
#37152=CARTESIAN_POINT('Ctrl Pts',(-22.8721695852919,20.399645221181,-8.58762627344358));
#37153=CARTESIAN_POINT('Ctrl Pts',(-22.8768518407422,20.3986410063383,-8.58792287663201));
#37154=CARTESIAN_POINT('Ctrl Pts',(-22.8792742344445,20.3981243899385,-8.58807612702932));
#37155=CARTESIAN_POINT('Ctrl Pts',(-22.8927668705227,20.3952631156596,-8.58892862941443));
#37156=CARTESIAN_POINT('Ctrl Pts',(-22.9038489912569,20.3929739437583,-8.5896247210007));
#37157=CARTESIAN_POINT('Ctrl Pts',(-23.0004243588922,20.3735547139665,-8.5956569219187));
#37158=CARTESIAN_POINT('Ctrl Pts',(-23.0865768106257,20.3598406542811,-8.60080737010682));
#37159=CARTESIAN_POINT('Ctrl Pts',(-23.3167410700854,20.3327249795871,-8.61420924637417));
#37160=CARTESIAN_POINT('Ctrl Pts',(-23.4612787620586,20.3254889682529,-8.62226231399615));
#37161=CARTESIAN_POINT('Ctrl Pts',(-23.8682045332157,20.3325065145344,-8.64500334971389));
#37162=CARTESIAN_POINT('Ctrl Pts',(-24.1290080314134,20.3690580132611,-8.65974601734649));
#37163=CARTESIAN_POINT('Ctrl Pts',(-24.3979730123308,20.4409528177106,-8.67662673108713));
#37164=CARTESIAN_POINT('Ctrl Pts',(-24.4134340220905,20.4452094684198,-8.67760274171195));
#37165=CARTESIAN_POINT('Ctrl Pts',(-24.4343240366428,20.4511288876333,-8.67892934456185));
#37166=CARTESIAN_POINT('Ctrl Pts',(-24.4397815426165,20.4526909221188,-8.67927664902685));
#37167=CARTESIAN_POINT('Ctrl Pts',(-24.4483722792125,20.4551743182147,-8.67982450664443));
#37168=CARTESIAN_POINT('Ctrl Pts',(-24.4515083031492,20.4560860425198,-8.6800247445866));
#37169=CARTESIAN_POINT('Ctrl Pts',(-24.4575469129457,20.4578515838417,-8.68041078782019));
#37170=CARTESIAN_POINT('Ctrl Pts',(-24.4604496943736,20.4587047249344,-8.68059657082713));
#37171=CARTESIAN_POINT('Ctrl Pts',(-24.4672976965006,20.4607278656806,-8.681035354133));
#37172=CARTESIAN_POINT('Ctrl Pts',(-24.4712418792818,20.4619013344399,-8.68128846783668));
#37173=CARTESIAN_POINT('Ctrl Pts',(-24.4793838911243,20.464340720936,-8.68181178637204));
#37174=CARTESIAN_POINT('Ctrl Pts',(-24.4835814038687,20.4656076570103,-8.68208202419808));
#37175=CARTESIAN_POINT('Ctrl Pts',(-24.5064330502439,20.4725558876646,-8.6835556762369));
#37176=CARTESIAN_POINT('Ctrl Pts',(-24.5250375885064,20.478397736488,-8.6847643556774));
#37177=CARTESIAN_POINT('Ctrl Pts',(-24.5729895746836,20.4939342030055,-8.68790323684717));
#37178=CARTESIAN_POINT('Ctrl Pts',(-24.6022520858705,20.5038826237384,-8.68984173337229));
#37179=CARTESIAN_POINT('Ctrl Pts',(-24.7256388101766,20.5478203595679,-8.69811559399015));
#37180=CARTESIAN_POINT('Ctrl Pts',(-24.8182876701456,20.5857601077218,-8.70457961761168));
#37181=CARTESIAN_POINT('Ctrl Pts',(-24.9864607687752,20.6639541957462,-8.71677962722367));
#37182=CARTESIAN_POINT('Ctrl Pts',(-25.0624407533349,20.7030262536865,-8.72247834415721));
#37183=CARTESIAN_POINT('Ctrl Pts',(-25.2065238551658,20.7845150538289,-8.73361391763236));
#37184=CARTESIAN_POINT('Ctrl Pts',(-25.2747756541109,20.826549520247,-8.73904131277138));
#37185=CARTESIAN_POINT('Ctrl Pts',(-25.5018475751631,20.9783565377205,-8.75752755849726));
#37186=CARTESIAN_POINT('Ctrl Pts',(-25.65236623206,21.0998425384074,-8.77055009609657));
#37187=CARTESIAN_POINT('Ctrl Pts',(-25.7993405518816,21.2420386158584,-8.78343687558731));
#37188=CARTESIAN_POINT('Ctrl Pts',(-25.8075191290508,21.2500360371797,-8.78415451414662));
#37189=CARTESIAN_POINT('Ctrl Pts',(-25.8181385178986,21.2605313898076,-8.78508681638621));
#37190=CARTESIAN_POINT('Ctrl Pts',(-25.8206179620484,21.2629898517747,-8.78530452816382));
#37191=CARTESIAN_POINT('Ctrl Pts',(-25.8244294142267,21.2667813537328,-8.7856392463875));
#37192=CARTESIAN_POINT('Ctrl Pts',(-25.8257642467635,21.2681115307367,-8.78575647910237));
#37193=CARTESIAN_POINT('Ctrl Pts',(-25.8284179200658,21.2707605917007,-8.78598955640326));
#37194=CARTESIAN_POINT('Ctrl Pts',(-25.8297367749204,21.2720794420927,-8.78610540182543));
#37195=CARTESIAN_POINT('Ctrl Pts',(-25.8326783833245,21.2750261523001,-8.78636380467813));
#37196=CARTESIAN_POINT('Ctrl Pts',(-25.8343005368991,21.2766545998514,-8.78650631388841));
#37197=CARTESIAN_POINT('Ctrl Pts',(-25.8376540028831,21.2800282882857,-8.78680095192132));
#37198=CARTESIAN_POINT('Ctrl Pts',(-25.839385064168,21.2817737782952,-8.78695306075394));
#37199=CARTESIAN_POINT('Ctrl Pts',(-25.8438710275129,21.2863074966391,-8.78734729198076));
#37200=CARTESIAN_POINT('Ctrl Pts',(-25.8466228533236,21.2890987836193,-8.78758917282893));
#37201=CARTESIAN_POINT('Ctrl Pts',(-25.8816200111191,21.3247275825165,-8.79066608053887));
#37202=CARTESIAN_POINT('Ctrl Pts',(-25.9131654859177,21.3582492172115,-8.79344729495734));
#37203=CARTESIAN_POINT('Ctrl Pts',(-26.0107764462834,21.466532081651,-8.80212277202728));
#37204=CARTESIAN_POINT('Ctrl Pts',(-26.0740984511117,21.5436947878039,-8.80785712787751));
#37205=CARTESIAN_POINT('Ctrl Pts',(-26.1569451001805,21.6547901149668,-8.81570628027586));
#37206=CARTESIAN_POINT('Ctrl Pts',(-26.1795834093834,21.6863203586925,-8.81789108470322));
#37207=CARTESIAN_POINT('Ctrl Pts',(-26.225230556148,21.7523839905228,-8.82239677430283));
#37208=CARTESIAN_POINT('Ctrl Pts',(-26.2481530125848,21.7869681634627,-8.82471623617704));
#37209=CARTESIAN_POINT('Ctrl Pts',(-26.4170307378308,22.0527676888526,-8.84231400873226));
#37210=CARTESIAN_POINT('Ctrl Pts',(-26.5336731708421,22.3012315860595,-8.85759716777871));
#37211=CARTESIAN_POINT('Ctrl Pts',(-26.6229787502142,22.5782525921642,-8.87522725900439));
#37212=CARTESIAN_POINT('Ctrl Pts',(-26.6282660744616,22.5951279808995,-8.8763028989983));
#37213=CARTESIAN_POINT('Ctrl Pts',(-26.6351342406631,22.6176983432464,-8.87774402651722));
#37214=CARTESIAN_POINT('Ctrl Pts',(-26.6368387618405,22.6233556033042,-8.87810545254564));
#37215=CARTESIAN_POINT('Ctrl Pts',(-26.639474550055,22.6321916103325,-8.87867029404943));
#37216=CARTESIAN_POINT('Ctrl Pts',(-26.6404164961137,22.6353671798997,-8.87887335954752));
#37217=CARTESIAN_POINT('Ctrl Pts',(-26.6422067852974,22.6414370647849,-8.87926163619824));
#37218=CARTESIAN_POINT('Ctrl Pts',(-26.6430559648271,22.6443311315879,-8.87944681976235));
#37219=CARTESIAN_POINT('Ctrl Pts',(-26.6450287232469,22.6510895418458,-8.87987940668242));
#37220=CARTESIAN_POINT('Ctrl Pts',(-26.6461491271297,22.6549548000691,-8.8801269135044));
#37221=CARTESIAN_POINT('Ctrl Pts',(-26.6484402906067,22.6629147660326,-8.88063683451766));
#37222=CARTESIAN_POINT('Ctrl Pts',(-26.64961017888,22.6670097143465,-8.88089927663189));
#37223=CARTESIAN_POINT('Ctrl Pts',(-26.6525882202093,22.6775124970252,-8.88157269708334));
#37224=CARTESIAN_POINT('Ctrl Pts',(-26.6543846323421,22.6839236143609,-8.88198405775232));
#37225=CARTESIAN_POINT('Ctrl Pts',(-26.6690070553294,22.7367381963858,-8.88537529190522));
#37226=CARTESIAN_POINT('Ctrl Pts',(-26.6808110645855,22.7834160307172,-8.8883882253994));
#37227=CARTESIAN_POINT('Ctrl Pts',(-26.7459135208793,23.0674877492968,-8.90683162709606));
#37228=CARTESIAN_POINT('Ctrl Pts',(-26.7732211168377,23.3099766345803,-8.92311349304411));
#37229=CARTESIAN_POINT('Ctrl Pts',(-26.773001214148,23.5531666769314,-8.93957441054318));
#37230=CARTESIAN_POINT('Ctrl Pts',(-26.7730012132604,23.5531676583652,-8.93957447697395));
#37231=CARTESIAN_POINT('Ctrl Pts',(-26.7728078658805,23.7669182373274,-8.95404271192202));
#37232=CARTESIAN_POINT('Ctrl Pts',(-26.7513493600371,23.980153034217,-8.96854767402835));
#37233=CARTESIAN_POINT('Ctrl Pts',(-26.7076087245426,24.1962117567834,-8.98241629501119));
#37234=CARTESIAN_POINT('Ctrl Pts',(-26.7062742060583,24.2027007225553,-8.98283199846243));
#37235=CARTESIAN_POINT('Ctrl Pts',(-26.7041939028601,24.2126602533808,-8.9834687320389));
#37236=CARTESIAN_POINT('Ctrl Pts',(-26.7034623869286,24.2161337310392,-8.98369055458102));
#37237=CARTESIAN_POINT('Ctrl Pts',(-26.7022468014455,24.2218588076012,-8.98405575755601));
#37238=CARTESIAN_POINT('Ctrl Pts',(-26.7017660569191,24.2241110975567,-8.98419932637149));
#37239=CARTESIAN_POINT('Ctrl Pts',(-26.7008240282472,24.2285014473913,-8.98447897540248));
#37240=CARTESIAN_POINT('Ctrl Pts',(-26.7003629811254,24.2306395561073,-8.98461506914724));
#37241=CARTESIAN_POINT('Ctrl Pts',(-26.6995445395715,24.2344164191022,-8.98485530054972));
#37242=CARTESIAN_POINT('Ctrl Pts',(-26.6991880443372,24.2360553553674,-8.98495948961635));
#37243=CARTESIAN_POINT('Ctrl Pts',(-26.6984240067506,24.2395547538723,-8.9851818283776));
#37244=CARTESIAN_POINT('Ctrl Pts',(-26.698016095785,24.2414151279678,-8.98529995612276));
#37245=CARTESIAN_POINT('Ctrl Pts',(-26.6968342144602,24.2467826280248,-8.98564056575428));
#37246=CARTESIAN_POINT('Ctrl Pts',(-26.6960560271926,24.2502888374825,-8.98586280407847));
#37247=CARTESIAN_POINT('Ctrl Pts',(-26.692587552028,24.2657938589516,-8.98684446565155));
#37248=CARTESIAN_POINT('Ctrl Pts',(-26.6898344180992,24.2777787243962,-8.98760030966766));
#37249=CARTESIAN_POINT('Ctrl Pts',(-26.6390311639475,24.49327385812,-9.00114252270274));
#37250=CARTESIAN_POINT('Ctrl Pts',(-26.5713463842603,24.6916831419501,-9.01285124716831));
#37251=CARTESIAN_POINT('Ctrl Pts',(-26.464828963232,24.9263774657351,-9.02725887432765));
#37252=CARTESIAN_POINT('Ctrl Pts',(-26.4437632472755,24.9701367998647,-9.02996950052121));
#37253=CARTESIAN_POINT('Ctrl Pts',(-26.399649666394,25.056710635031,-9.0354071566973));
#37254=CARTESIAN_POINT('Ctrl Pts',(-26.376605841805,25.0995126448388,-9.03813348394425));
#37255=CARTESIAN_POINT('Ctrl Pts',(-26.2838173315237,25.2628943667709,-9.04873352151199));
#37256=CARTESIAN_POINT('Ctrl Pts',(-26.2072588814237,25.3794134888963,-9.05671690527982));
#37257=CARTESIAN_POINT('Ctrl Pts',(-26.0899619278102,25.5349640794995,-9.06827346276721));
#37258=CARTESIAN_POINT('Ctrl Pts',(-26.0553746749621,25.5784453768402,-9.07160982174604));
#37259=CARTESIAN_POINT('Ctrl Pts',(-26.0152241238418,25.6263259305737,-9.07541410948211));
#37260=CARTESIAN_POINT('Ctrl Pts',(-26.0107485965919,25.6316282356625,-9.07583724079194));
#37261=CARTESIAN_POINT('Ctrl Pts',(-26.003421959669,25.6402516892807,-9.07652843851192));
#37262=CARTESIAN_POINT('Ctrl Pts',(-26.0005811297096,25.6435815747527,-9.07679608200145));
#37263=CARTESIAN_POINT('Ctrl Pts',(-25.9950598925253,25.6500266671777,-9.0773155614169));
#37264=CARTESIAN_POINT('Ctrl Pts',(-25.9923802916666,25.6531425562419,-9.07756736374422));
#37265=CARTESIAN_POINT('Ctrl Pts',(-25.9877180204353,25.6585430012168,-9.07800493676978));
#37266=CARTESIAN_POINT('Ctrl Pts',(-25.9857380754591,25.6608299121036,-9.07819059415372));
#37267=CARTESIAN_POINT('Ctrl Pts',(-25.9816121138658,25.665582016023,-9.07857713320096));
#37268=CARTESIAN_POINT('Ctrl Pts',(-25.9794655617997,25.6680467377801,-9.07877803705164));
#37269=CARTESIAN_POINT('Ctrl Pts',(-25.9735721735892,25.6747929162054,-9.07932909074726));
#37270=CARTESIAN_POINT('Ctrl Pts',(-25.9698177565168,25.6790677078844,-9.07967955711122));
#37271=CARTESIAN_POINT('Ctrl Pts',(-25.9553795957711,25.6954195100647,-9.08102510925123));
#37272=CARTESIAN_POINT('Ctrl Pts',(-25.9446167306384,25.7074260590344,-9.08202351509584));
#37273=CARTESIAN_POINT('Ctrl Pts',(-25.7568582072712,25.9137443230065,-9.09936318920441));
#37274=CARTESIAN_POINT('Ctrl Pts',(-25.5568754223864,26.0857225123447,-9.1167758909787));
#37275=CARTESIAN_POINT('Ctrl Pts',(-25.2737376435289,26.2745391199642,-9.13979081734646));
#37276=CARTESIAN_POINT('Ctrl Pts',(-25.2076479312285,26.3152442045469,-9.14505203024023));
#37277=CARTESIAN_POINT('Ctrl Pts',(-25.0641567443149,26.3966265173592,-9.15617563231805));
#37278=CARTESIAN_POINT('Ctrl Pts',(-24.9864343343809,26.4366229864699,-9.1620260472387));
#37279=CARTESIAN_POINT('Ctrl Pts',(-24.8605846304507,26.4950421937532,-9.17113274904898));
#37280=CARTESIAN_POINT('Ctrl Pts',(-24.8134772370519,26.5155552756975,-9.17446304808412));
#37281=CARTESIAN_POINT('Ctrl Pts',(-24.7509119592197,26.5410377622456,-9.17876570665235));
#37282=CARTESIAN_POINT('Ctrl Pts',(-24.7358810454088,26.5470282004189,-9.17979039023191));
#37283=CARTESIAN_POINT('Ctrl Pts',(-24.7112636828298,26.5566250215961,-9.18145319655281));
#37284=CARTESIAN_POINT('Ctrl Pts',(-24.7017042361781,26.5602992788561,-9.18209513238091));
#37285=CARTESIAN_POINT('Ctrl Pts',(-24.6898792421018,26.5647797421613,-9.18288441629445));
#37286=CARTESIAN_POINT('Ctrl Pts',(-24.6876302385443,26.5656290079855,-9.18303431745502));
#37287=CARTESIAN_POINT('Ctrl Pts',(-24.6832655598858,26.5672716144754,-9.18332481661476));
#37288=CARTESIAN_POINT('Ctrl Pts',(-24.6811499974788,26.5680652478638,-9.18346543213911));
#37289=CARTESIAN_POINT('Ctrl Pts',(-24.6773046698804,26.5695031750614,-9.1837206736744));
#37290=CARTESIAN_POINT('Ctrl Pts',(-24.6755751928137,26.5701482050711,-9.18383534382065));
#37291=CARTESIAN_POINT('Ctrl Pts',(-24.6720609766479,26.5714554376694,-9.18406808936415));
#37292=CARTESIAN_POINT('Ctrl Pts',(-24.6702762119692,26.572117542232,-9.18418615858885));
#37293=CARTESIAN_POINT('Ctrl Pts',(-24.6651269111073,26.5740226197903,-9.18452641809959));
#37294=CARTESIAN_POINT('Ctrl Pts',(-24.6617608714587,26.5752615628324,-9.1847483656156));
#37295=CARTESIAN_POINT('Ctrl Pts',(-24.6468850206994,26.5807087566014,-9.1857271658962));
#37296=CARTESIAN_POINT('Ctrl Pts',(-24.6353531305201,26.5848570279695,-9.18648046492864));
#37297=CARTESIAN_POINT('Ctrl Pts',(-24.4374462254037,26.6547760398833,-9.19931931277185));
#37298=CARTESIAN_POINT('Ctrl Pts',(-24.245401182448,26.7033419201677,-9.21044159575959));
#37299=CARTESIAN_POINT('Ctrl Pts',(-23.8767040662614,26.7612259883571,-9.23132255251582));
#37300=CARTESIAN_POINT('Ctrl Pts',(-23.7013883070317,26.7742369283798,-9.24106370529646));
#37301=CARTESIAN_POINT('Ctrl Pts',(-23.4097268643695,26.772032440428,-9.25785337287125));
#37302=CARTESIAN_POINT('Ctrl Pts',(-23.2937035648919,26.7648740164228,-9.26468166520517));
#37303=CARTESIAN_POINT('Ctrl Pts',(-23.1595200641905,26.7492842963919,-9.27285945600781));
#37304=CARTESIAN_POINT('Ctrl Pts',(-23.1407316302965,26.7469334197694,-9.27401084508389));
#37305=CARTESIAN_POINT('Ctrl Pts',(-23.116137701976,26.7436357609215,-9.27552664793765));
#37306=CARTESIAN_POINT('Ctrl Pts',(-23.1103122736418,26.7428384275961,-9.27588632421064));
#37307=CARTESIAN_POINT('Ctrl Pts',(-23.1008504631222,26.7415169897278,-9.27647156531165));
#37308=CARTESIAN_POINT('Ctrl Pts',(-23.0972127196351,26.7410025985057,-9.27669682190857));
#37309=CARTESIAN_POINT('Ctrl Pts',(-23.0902333866196,26.7400035172467,-9.2771294821972));
#37310=CARTESIAN_POINT('Ctrl Pts',(-23.0868916618299,26.7395197935914,-9.27733685496387));
#37311=CARTESIAN_POINT('Ctrl Pts',(-23.0792728966128,26.7384047296838,-9.2778101324272));
#37312=CARTESIAN_POINT('Ctrl Pts',(-23.0749963606751,26.7377700337362,-9.27807614332407));
#37313=CARTESIAN_POINT('Ctrl Pts',(-23.0616750714806,26.7357655691576,-9.2789058664102));
#37314=CARTESIAN_POINT('Ctrl Pts',(-23.0526349239343,26.7343659028161,-9.27947052715836));
#37315=CARTESIAN_POINT('Ctrl Pts',(-22.9824787258578,26.7231977039833,-9.28386511231251));
#37316=CARTESIAN_POINT('Ctrl Pts',(-22.9216532304913,26.711709509106,-9.28774949674526));
#37317=CARTESIAN_POINT('Ctrl Pts',(-22.856311438363,26.6974081297277,-9.29200721751513));
#37318=CARTESIAN_POINT('Ctrl Pts',(-22.8514259926214,26.6963269216426,-9.29232607112002));
#37319=CARTESIAN_POINT('Ctrl Pts',(-22.8317451799987,26.6919232162596,-9.29361263621379));
#37320=CARTESIAN_POINT('Ctrl Pts',(-22.8169710086694,26.6885077316994,-9.2945831825999));
#37321=CARTESIAN_POINT('Ctrl Pts',(-22.7744183989526,26.6783535533502,-9.29739226507565));
#37322=CARTESIAN_POINT('Ctrl Pts',(-22.746705307041,26.6713495154611,-9.29923865653612));
#37323=CARTESIAN_POINT('Ctrl Pts',(-22.598495483465,26.6317871005532,-9.30920377958813));
#37324=CARTESIAN_POINT('Ctrl Pts',(-22.4798841145426,26.5926205362366,-9.31750789520908));
#37325=CARTESIAN_POINT('Ctrl Pts',(-22.2654847629832,26.5077315882893,-9.33303371024729));
#37326=CARTESIAN_POINT('Ctrl Pts',(-22.1690958172653,26.4639642817613,-9.34021715872359));
#37327=CARTESIAN_POINT('Ctrl Pts',(-22.075036015341,26.4155367745536,-9.34735996012824));
#37328=CARTESIAN_POINT('',(-26.7730021134982,23.5486107394123,-9.18577344932659));
#37329=CARTESIAN_POINT('Ctrl Pts',(-22.0750360153461,26.4155367745563,-9.59296972147339));
#37330=CARTESIAN_POINT('Ctrl Pts',(-22.1637577963692,26.4612159552698,-9.58679793631509));
#37331=CARTESIAN_POINT('Ctrl Pts',(-22.2544891503987,26.5027117903437,-9.58062615115677));
#37332=CARTESIAN_POINT('Ctrl Pts',(-22.346794125753,26.5398687993228,-9.57445436599846));
#37333=CARTESIAN_POINT('Ctrl Pts',(-22.3879140852554,26.5564214791603,-9.57170496321933));
#37334=CARTESIAN_POINT('Ctrl Pts',(-22.4293461334093,26.5721137747017,-9.56895556044019));
#37335=CARTESIAN_POINT('Ctrl Pts',(-22.4710509224819,26.5869351705575,-9.56620615766106));
#37336=CARTESIAN_POINT('Ctrl Pts',(-22.5646733514219,26.6202074903835,-9.56003406634873));
#37337=CARTESIAN_POINT('Ctrl Pts',(-22.6600008140785,26.6492047142014,-9.5538619750364));
#37338=CARTESIAN_POINT('Ctrl Pts',(-22.7566065109273,26.6737511400212,-9.54768988372408));
#37339=CARTESIAN_POINT('Ctrl Pts',(-22.8530813166075,26.6982643078607,-9.54152615498529));
#37340=CARTESIAN_POINT('Ctrl Pts',(-22.95083049687,26.7183385577121,-9.5353624262465));
#37341=CARTESIAN_POINT('Ctrl Pts',(-23.0494092502704,26.7338469735088,-9.52919869750771));
#37342=CARTESIAN_POINT('Ctrl Pts',(-23.1478835687336,26.7493389595945,-9.52304149866104));
#37343=CARTESIAN_POINT('Ctrl Pts',(-23.2471852863367,26.7602746610277,-9.51688429981437));
#37344=CARTESIAN_POINT('Ctrl Pts',(-23.3468574210034,26.7665777626755,-9.5107271009677));
#37345=CARTESIAN_POINT('Ctrl Pts',(-23.4464567013842,26.7728762571383,-9.50457440266));
#37346=CARTESIAN_POINT('Ctrl Pts',(-23.5464254283002,26.7745488567173,-9.4984217043523));
#37347=CARTESIAN_POINT('Ctrl Pts',(-23.6463003894648,26.7715709530114,-9.49226900604459));
#37348=CARTESIAN_POINT('Ctrl Pts',(-23.7461374779021,26.7685941785308,-9.48611864084884));
#37349=CARTESIAN_POINT('Ctrl Pts',(-23.8458804375116,26.7609704177089,-9.47996827565307));
#37350=CARTESIAN_POINT('Ctrl Pts',(-23.9450658330466,26.7487271712021,-9.47381791045731));
#37351=CARTESIAN_POINT('Ctrl Pts',(-24.0442401523507,26.7364852919231,-9.4676682320851));
#37352=CARTESIAN_POINT('Ctrl Pts',(-24.1428566002399,26.719625005791,-9.46151855371289));
#37353=CARTESIAN_POINT('Ctrl Pts',(-24.2404576488375,26.6982256031751,-9.45536887534068));
#37354=CARTESIAN_POINT('Ctrl Pts',(-24.3380739090803,26.676822865348,-9.44921823850822));
#37355=CARTESIAN_POINT('Ctrl Pts',(-24.4346740313327,26.6508796989122,-9.44306760167575));
#37356=CARTESIAN_POINT('Ctrl Pts',(-24.5298124422281,26.6205261260462,-9.43691696484329));
#37357=CARTESIAN_POINT('Ctrl Pts',(-24.6250526312376,26.5901400812334,-9.43075974812147));
#37358=CARTESIAN_POINT('Ctrl Pts',(-24.7188275716294,26.5553343404886,-9.42460253139967));
#37359=CARTESIAN_POINT('Ctrl Pts',(-24.8107086959699,26.5162882395776,-9.41844531467785));
#37360=CARTESIAN_POINT('Ctrl Pts',(-24.9026410804132,26.4772203550069,-9.41228466287005));
#37361=CARTESIAN_POINT('Ctrl Pts',(-24.9926771532215,26.4339075873789,-9.40612401106223));
#37362=CARTESIAN_POINT('Ctrl Pts',(-25.0804120134834,26.3865757718752,-9.39996335925443));
#37363=CARTESIAN_POINT('Ctrl Pts',(-25.1682936853654,26.3391647534127,-9.39379239848539));
#37364=CARTESIAN_POINT('Ctrl Pts',(-25.2538660804435,26.2877214773809,-9.38762143771638));
#37365=CARTESIAN_POINT('Ctrl Pts',(-25.3367522804116,26.2325157943761,-9.38145047694735));
#37366=CARTESIAN_POINT('Ctrl Pts',(-25.400020873111,26.1903762600016,-9.37674006672694));
#37367=CARTESIAN_POINT('Ctrl Pts',(-25.4617249171379,26.1460454492973,-9.37202965650652));
#37368=CARTESIAN_POINT('Ctrl Pts',(-25.5217103655992,26.0996586530556,-9.36731924628612));
#37369=CARTESIAN_POINT('Ctrl Pts',(-25.5994036959404,26.0395783373067,-9.36121830903075));
#37370=CARTESIAN_POINT('Ctrl Pts',(-25.6745002405137,25.9758253033282,-9.35511737177537));
#37371=CARTESIAN_POINT('Ctrl Pts',(-25.7466261173724,25.9086546675979,-9.34901643452001));
#37372=CARTESIAN_POINT('Ctrl Pts',(-25.8186539201148,25.8415753680292,-9.34292379309488));
#37373=CARTESIAN_POINT('Ctrl Pts',(-25.8877187567366,25.77108799903,-9.33683115166976));
#37374=CARTESIAN_POINT('Ctrl Pts',(-25.9534776244252,25.6974895275026,-9.33073851024463));
#37375=CARTESIAN_POINT('Ctrl Pts',(-26.0191620495435,25.623974373398,-9.32465276601684));
#37376=CARTESIAN_POINT('Ctrl Pts',(-26.0815476510511,25.547355448728,-9.31856702178908));
#37377=CARTESIAN_POINT('Ctrl Pts',(-26.1403272040665,25.4679675141761,-9.31248127756129));
#37378=CARTESIAN_POINT('Ctrl Pts',(-26.1990701315555,25.3886290462285,-9.30639932535937));
#37379=CARTESIAN_POINT('Ctrl Pts',(-26.2542112077898,25.3065253510947,-9.30031737315742));
#37380=CARTESIAN_POINT('Ctrl Pts',(-26.3054831090182,25.2220246538086,-9.2942354209555));
#37381=CARTESIAN_POINT('Ctrl Pts',(-26.3567375395523,25.1375527497956,-9.28815554115435));
#37382=CARTESIAN_POINT('Ctrl Pts',(-26.4041251830893,25.0506858464732,-9.28207566135319));
#37383=CARTESIAN_POINT('Ctrl Pts',(-26.4474223844702,24.9618205983017,-9.27599578155204));
#37384=CARTESIAN_POINT('Ctrl Pts',(-26.4907170569699,24.8729605405267,-9.26991625686144));
#37385=CARTESIAN_POINT('Ctrl Pts',(-26.5299215681555,24.7821027708259,-9.26383673217088));
#37386=CARTESIAN_POINT('Ctrl Pts',(-26.5648590466163,24.6896669087711,-9.25775720748028));
#37387=CARTESIAN_POINT('Ctrl Pts',(-26.5998254795955,24.5971544402755,-9.25167264436913));
#37388=CARTESIAN_POINT('Ctrl Pts',(-26.6305176570152,24.5030616840487,-9.24558808125795));
#37389=CARTESIAN_POINT('Ctrl Pts',(-26.6568076885387,24.4078262136498,-9.23950351814679));
#37390=CARTESIAN_POINT('Ctrl Pts',(-26.6831081413057,24.312552992363,-9.23341654314373));
#37391=CARTESIAN_POINT('Ctrl Pts',(-26.7050028737611,24.2161365894468,-9.22732956814067));
#37392=CARTESIAN_POINT('Ctrl Pts',(-26.7224150143323,24.1190255499041,-9.2212425931376));
#37393=CARTESIAN_POINT('Ctrl Pts',(-26.739854639304,24.0217612242846,-9.21514601007636));
#37394=CARTESIAN_POINT('Ctrl Pts',(-26.7527974776387,23.9238005137262,-9.20904942701514));
#37395=CARTESIAN_POINT('Ctrl Pts',(-26.7612185047024,23.8255979196766,-9.2029528439539));
#37396=CARTESIAN_POINT('Ctrl Pts',(-26.7691282986336,23.7333571185777,-9.19722637907812));
#37397=CARTESIAN_POINT('Ctrl Pts',(-26.7730491308417,23.6409032453324,-9.19149991420236));
#37398=CARTESIAN_POINT('Ctrl Pts',(-26.7730021134982,23.5486107394123,-9.18577344932659));
#37399=CARTESIAN_POINT('Ctrl Pts',(-26.7730021922999,23.5487734894733,-9.18330474046535));
#37400=CARTESIAN_POINT('Ctrl Pts',(-26.7729649266428,23.4675737224467,-9.17795163051465));
#37401=CARTESIAN_POINT('Ctrl Pts',(-26.7698588128614,23.3863948059531,-9.17269397152322));
#37402=CARTESIAN_POINT('Ctrl Pts',(-26.7633169126019,23.3005351682824,-9.16729179848125));
#37403=CARTESIAN_POINT('Ctrl Pts',(-26.7629342824696,23.2956598247637,-9.16698559405237));
#37404=CARTESIAN_POINT('Ctrl Pts',(-26.7623102620737,23.2879342499821,-9.16650126107428));
#37405=CARTESIAN_POINT('Ctrl Pts',(-26.7620761738631,23.2850834611615,-9.16632273006705));
#37406=CARTESIAN_POINT('Ctrl Pts',(-26.7616705729007,23.2802232849545,-9.1660186911729));
#37407=CARTESIAN_POINT('Ctrl Pts',(-26.7615009694366,23.2782137465336,-9.16589307641493));
#37408=CARTESIAN_POINT('Ctrl Pts',(-26.761180922018,23.2744636872304,-9.16565884438339));
#37409=CARTESIAN_POINT('Ctrl Pts',(-26.7610309489815,23.2727231285041,-9.16555020048642));
#37410=CARTESIAN_POINT('Ctrl Pts',(-26.7607160796995,23.2691032323758,-9.16532440321754));
#37411=CARTESIAN_POINT('Ctrl Pts',(-26.7605509489693,23.2672239224816,-9.16520726401055));
#37412=CARTESIAN_POINT('Ctrl Pts',(-26.7601674312223,23.2629027261268,-9.16493811570678));
#37413=CARTESIAN_POINT('Ctrl Pts',(-26.7599479073948,23.2604609371394,-9.16478617129267));
#37414=CARTESIAN_POINT('Ctrl Pts',(-26.7592423597792,23.2527122058869,-9.1643044434345));
#37415=CARTESIAN_POINT('Ctrl Pts',(-26.7587459556855,23.2474061821959,-9.1639752452407));
#37416=CARTESIAN_POINT('Ctrl Pts',(-26.7544055259695,23.2022204741573,-9.16117733973073));
#37417=CARTESIAN_POINT('Ctrl Pts',(-26.7498310951871,23.1624122281876,-9.15874905338377));
#37418=CARTESIAN_POINT('Ctrl Pts',(-26.7435922082235,23.1158015235292,-9.15593805988852));
#37419=CARTESIAN_POINT('Ctrl Pts',(-26.7426468465274,23.1089085519481,-9.1555231895877));
#37420=CARTESIAN_POINT('Ctrl Pts',(-26.7403632336336,23.0926492215005,-9.15454642879065));
#37421=CARTESIAN_POINT('Ctrl Pts',(-26.739006036729,23.0832855434019,-9.15398536417351));
#37422=CARTESIAN_POINT('Ctrl Pts',(-26.7347395263774,23.0547359327775,-9.15227874412316));
#37423=CARTESIAN_POINT('Ctrl Pts',(-26.7316981041866,23.0355698926794,-9.15113863751684));
#37424=CARTESIAN_POINT('Ctrl Pts',(-26.7264224409202,23.0041599339501,-9.14927767978094));
#37425=CARTESIAN_POINT('Ctrl Pts',(-26.7242901010063,22.9918996564146,-9.14855316945212));
#37426=CARTESIAN_POINT('Ctrl Pts',(-26.6687491844894,22.6831608109983,-9.13034912425828));
#37427=CARTESIAN_POINT('Ctrl Pts',(-26.574104119805,22.3956005397989,-9.11419674428456));
#37428=CARTESIAN_POINT('Ctrl Pts',(-26.4044584708247,22.0514481553201,-9.09205387220421));
#37429=CARTESIAN_POINT('Ctrl Pts',(-26.365211361839,21.9789755759874,-9.08722616546257));
#37430=CARTESIAN_POINT('Ctrl Pts',(-26.3014680966286,21.8713377242562,-9.07974840919229));
#37431=CARTESIAN_POINT('Ctrl Pts',(-26.278975578972,21.8350230194398,-9.0771701361137));
#37432=CARTESIAN_POINT('Ctrl Pts',(-26.2516358852398,21.7927817935061,-9.07410109388587));
#37433=CARTESIAN_POINT('Ctrl Pts',(-26.2474804236841,21.7864109527796,-9.07363631364378));
#37434=CARTESIAN_POINT('Ctrl Pts',(-26.2410751656187,21.7766664588255,-9.07292245884629));
#37435=CARTESIAN_POINT('Ctrl Pts',(-26.2388414710478,21.77328221116,-9.07267398967577));
#37436=CARTESIAN_POINT('Ctrl Pts',(-26.2349335340921,21.7673855728142,-9.07224010058451));
#37437=CARTESIAN_POINT('Ctrl Pts',(-26.2332621336659,21.7648712969623,-9.07205478796363));
#37438=CARTESIAN_POINT('Ctrl Pts',(-26.2294935717123,21.7592195185919,-9.07163753711554));
#37439=CARTESIAN_POINT('Ctrl Pts',(-26.2273944299449,21.7560833476492,-9.0714055242391));
#37440=CARTESIAN_POINT('Ctrl Pts',(-26.2217620660332,21.7477003456505,-9.07078406090117));
#37441=CARTESIAN_POINT('Ctrl Pts',(-26.2182189099997,21.7424602375427,-9.07039423440136));
#37442=CARTESIAN_POINT('Ctrl Pts',(-26.202851021567,21.719875666319,-9.06870819765479));
#37443=CARTESIAN_POINT('Ctrl Pts',(-26.1908726219754,21.7026368457372,-9.06740614724789));
#37444=CARTESIAN_POINT('Ctrl Pts',(-25.9737854548101,21.3966374588687,-9.04401825098519));
#37445=CARTESIAN_POINT('Ctrl Pts',(-25.7226547628741,21.1435739184067,-9.01985039402449));
#37446=CARTESIAN_POINT('Ctrl Pts',(-25.3900387374496,20.9036598339824,-8.99229640199206));
#37447=CARTESIAN_POINT('Ctrl Pts',(-25.343677956174,20.872027012824,-8.98854996608669));
#37448=CARTESIAN_POINT('Ctrl Pts',(-25.2460959987815,20.8091157424671,-8.98088864145837));
#37449=CARTESIAN_POINT('Ctrl Pts',(-25.1947775592959,20.7780233945862,-8.97698133965448));
#37450=CARTESIAN_POINT('Ctrl Pts',(-25.1267771519296,20.7393772849319,-8.97198858415305));
#37451=CARTESIAN_POINT('Ctrl Pts',(-25.1108601166761,20.7305090093033,-8.97083278581258));
#37452=CARTESIAN_POINT('Ctrl Pts',(-25.0883189643709,20.7181994077409,-8.96921495456499));
#37453=CARTESIAN_POINT('Ctrl Pts',(-25.0817571402663,20.7146455623265,-8.96874624401838));
#37454=CARTESIAN_POINT('Ctrl Pts',(-25.0702870907136,20.7084848799883,-8.9679309312077));
#37455=CARTESIAN_POINT('Ctrl Pts',(-25.0653843883001,20.7058679049089,-8.96758370437275));
#37456=CARTESIAN_POINT('Ctrl Pts',(-25.0582540130377,20.702085504463,-8.96708057006287));
#37457=CARTESIAN_POINT('Ctrl Pts',(-25.0560317416068,20.7009100015937,-8.96692402421141));
#37458=CARTESIAN_POINT('Ctrl Pts',(-25.0522399119569,20.6989099329514,-8.9666573622799));
#37459=CARTESIAN_POINT('Ctrl Pts',(-25.0506710473117,20.6980840612277,-8.96654716242713));
#37460=CARTESIAN_POINT('Ctrl Pts',(-25.0475485934068,20.6964436482609,-8.96632809766881));
#37461=CARTESIAN_POINT('Ctrl Pts',(-25.0459950223811,20.6956290817145,-8.96621923114136));
#37462=CARTESIAN_POINT('Ctrl Pts',(-25.042333267798,20.6937129647931,-8.96596293492282));
#37463=CARTESIAN_POINT('Ctrl Pts',(-25.0402245247658,20.6926124773362,-8.96581557329073));
#37464=CARTESIAN_POINT('Ctrl Pts',(-25.0339914062557,20.6893683816372,-8.96538068336349));
#37465=CARTESIAN_POINT('Ctrl Pts',(-25.029863586841,20.6872313487374,-8.96509357111276));
#37466=CARTESIAN_POINT('Ctrl Pts',(-24.9938442019695,20.6686822868985,-8.96259584311043));
#37467=CARTESIAN_POINT('Ctrl Pts',(-24.9616837346014,20.6527939541939,-8.96041767060814));
#37468=CARTESIAN_POINT('Ctrl Pts',(-24.9207730841527,20.6334256232266,-8.95770351342188));
#37469=CARTESIAN_POINT('Ctrl Pts',(-24.9122654365868,20.6294432860069,-8.9571421401036));
#37470=CARTESIAN_POINT('Ctrl Pts',(-24.9001979581806,20.6238588219682,-8.95635001941079));
#37471=CARTESIAN_POINT('Ctrl Pts',(-24.8966525242109,20.6222259165062,-8.95611779853653));
#37472=CARTESIAN_POINT('Ctrl Pts',(-24.8906626029107,20.6194803438804,-8.95572630425528));
#37473=CARTESIAN_POINT('Ctrl Pts',(-24.8882196842982,20.6183642878274,-8.95556687249244));
#37474=CARTESIAN_POINT('Ctrl Pts',(-24.8727428252294,20.6113170018099,-8.95455827579723));
#37475=CARTESIAN_POINT('Ctrl Pts',(-24.8596706704911,20.6054695556475,-8.95371297050655));
#37476=CARTESIAN_POINT('Ctrl Pts',(-24.7046465692939,20.5373604476481,-8.94376106003376));
#37477=CARTESIAN_POINT('Ctrl Pts',(-24.5584067237617,20.4853254409156,-8.93508396744657));
#37478=CARTESIAN_POINT('Ctrl Pts',(-24.3920097949483,20.4393246630043,-8.92543455881836));
#37479=CARTESIAN_POINT('Ctrl Pts',(-24.3750032243837,20.4347728270614,-8.92445097898462));
#37480=CARTESIAN_POINT('Ctrl Pts',(-24.338385557134,20.4252928927794,-8.92233748122336));
#37481=CARTESIAN_POINT('Ctrl Pts',(-24.3187636758423,20.4204095596233,-8.92120757663564));
#37482=CARTESIAN_POINT('Ctrl Pts',(-24.2761361980358,20.410225818253,-8.91875661257138));
#37483=CARTESIAN_POINT('Ctrl Pts',(-24.2531157422147,20.4049928990619,-8.91743531402306));
#37484=CARTESIAN_POINT('Ctrl Pts',(-24.2024403855555,20.3940577067689,-8.91452871945726));
#37485=CARTESIAN_POINT('Ctrl Pts',(-24.1747639545671,20.3884650266642,-8.91294257605036));
#37486=CARTESIAN_POINT('Ctrl Pts',(-24.1124570050957,20.3767244391647,-8.90936962071323));
#37487=CARTESIAN_POINT('Ctrl Pts',(-24.0777924086686,20.3707783564588,-8.90738032007583));
#37488=CARTESIAN_POINT('Ctrl Pts',(-23.8808558805949,20.3403067809584,-8.89604786125396));
#37489=CARTESIAN_POINT('Ctrl Pts',(-23.7170172113642,20.3276405363788,-8.88648452576365));
#37490=CARTESIAN_POINT('Ctrl Pts',(-23.5424676569154,20.3274949155151,-8.87586075863551));
#37491=CARTESIAN_POINT('Ctrl Pts',(-23.5319942686975,20.327537234204,-8.8752217168117));
#37492=CARTESIAN_POINT('Ctrl Pts',(-23.5169019141914,20.3276717895139,-8.87429849408435));
#37493=CARTESIAN_POINT('Ctrl Pts',(-23.5122825724061,20.3277229064775,-8.87401560439957));
#37494=CARTESIAN_POINT('Ctrl Pts',(-23.5042518243662,20.3278290433645,-8.87352324180883));
#37495=CARTESIAN_POINT('Ctrl Pts',(-23.5008403574974,20.3278795489205,-8.8733139109486));
#37496=CARTESIAN_POINT('Ctrl Pts',(-23.4942710364588,20.3279872400047,-8.87291047184784));
#37497=CARTESIAN_POINT('Ctrl Pts',(-23.491113171878,20.3280436505325,-8.87271638817393));
#37498=CARTESIAN_POINT('Ctrl Pts',(-23.4836590482543,20.3281877688383,-8.87225789589132));
#37499=CARTESIAN_POINT('Ctrl Pts',(-23.4793628789961,20.328279427378,-8.87199336344817));
#37500=CARTESIAN_POINT('Ctrl Pts',(-23.4644339130206,20.3286278096574,-8.87107314097701));
#37501=CARTESIAN_POINT('Ctrl Pts',(-23.4538023014709,20.3289285750448,-8.8704160693096));
#37502=CARTESIAN_POINT('Ctrl Pts',(-23.3248658067932,20.3332150243829,-8.8624258434317));
#37503=CARTESIAN_POINT('Ctrl Pts',(-23.2068800103227,20.343662610776,-8.85488955474929));
#37504=CARTESIAN_POINT('Ctrl Pts',(-22.8190818270482,20.399650403051,-8.82933627767633));
#37505=CARTESIAN_POINT('Ctrl Pts',(-22.5545049586475,20.4730207294435,-8.81052096007095));
#37506=CARTESIAN_POINT('Ctrl Pts',(-22.2389584925178,20.6055345853877,-8.78767410165781));
#37507=CARTESIAN_POINT('Ctrl Pts',(-22.1763585486276,20.6342154297348,-8.78312788799295));
#37508=CARTESIAN_POINT('Ctrl Pts',(-22.0934938065402,20.6754423225323,-8.77713375490202));
#37509=CARTESIAN_POINT('Ctrl Pts',(-22.0723825397473,20.6862378532114,-8.77560881045344));
#37510=CARTESIAN_POINT('Ctrl Pts',(-22.0357566163987,20.7054798495902,-8.7729694239255));
#37511=CARTESIAN_POINT('Ctrl Pts',(-22.0201889132558,20.7138225843706,-8.77184955930556));
#37512=CARTESIAN_POINT('Ctrl Pts',(-21.9982907497336,20.7257905696615,-8.77027798104856));
#37513=CARTESIAN_POINT('Ctrl Pts',(-21.99190313113,20.7293097999446,-8.76982000190449));
#37514=CARTESIAN_POINT('Ctrl Pts',(-21.982200691393,20.7346983287807,-8.76912509926341));
#37515=CARTESIAN_POINT('Ctrl Pts',(-21.9788771960467,20.7365518371841,-8.76888719883389));
#37516=CARTESIAN_POINT('Ctrl Pts',(-21.9727505856843,20.7399828793852,-8.76844890443323));
#37517=CARTESIAN_POINT('Ctrl Pts',(-21.9699465398368,20.741558728399,-8.76824840407281));
#37518=CARTESIAN_POINT('Ctrl Pts',(-21.9653888494244,20.7441290961766,-8.76792267924017));
#37519=CARTESIAN_POINT('Ctrl Pts',(-21.9636337793284,20.7451210621488,-8.76779729011604));
#37520=CARTESIAN_POINT('Ctrl Pts',(-21.9602399627658,20.7470434520324,-8.76755490284713));
#37521=CARTESIAN_POINT('Ctrl Pts',(-21.9586011065491,20.7479736636127,-8.7674378918529));
#37522=CARTESIAN_POINT('Ctrl Pts',(-21.9548440797919,20.7501105037488,-8.76716973002253));
#37523=CARTESIAN_POINT('Ctrl Pts',(-21.9527264569436,20.7513181012987,-8.7670186423069));
#37524=CARTESIAN_POINT('Ctrl Pts',(-21.9460476718936,20.7551368002395,-8.76654230830306));
#37525=CARTESIAN_POINT('Ctrl Pts',(-21.9414914958475,20.7577566740606,-8.76621762880174));
#37526=CARTESIAN_POINT('Ctrl Pts',(-21.9039093894471,20.7794894900426,-8.7635415280146));
#37527=CARTESIAN_POINT('Ctrl Pts',(-21.8712171353014,20.7991774642645,-8.76122673372378));
#37528=CARTESIAN_POINT('Ctrl Pts',(-21.8358320149225,20.8213529736959,-8.75872702475207));
#37529=CARTESIAN_POINT('Ctrl Pts',(-21.832786674081,20.8232685687535,-8.75851194021225));
#37530=CARTESIAN_POINT('Ctrl Pts',(-21.5974611074795,20.9718447595649,-8.74189465095875));
#37531=CARTESIAN_POINT('Ctrl Pts',(-21.3848504492797,21.1476168511753,-8.72704117392225));
#37532=CARTESIAN_POINT('Ctrl Pts',(-21.17094083591,21.3762104220449,-8.7093772359835));
#37533=CARTESIAN_POINT('Ctrl Pts',(-21.1452832006768,21.4046277603611,-8.70720780803039));
#37534=CARTESIAN_POINT('Ctrl Pts',(-21.0477981627449,21.5165441077007,-8.69874533626598));
#37535=CARTESIAN_POINT('Ctrl Pts',(-20.9797689921945,21.6032397648594,-8.69235779787456));
#37536=CARTESIAN_POINT('Ctrl Pts',(-20.8879039828806,21.7335387954449,-8.68285902140014));
#37537=CARTESIAN_POINT('Ctrl Pts',(-20.8604229900186,21.7744808053182,-8.6798884549838));
#37538=CARTESIAN_POINT('Ctrl Pts',(-20.8296407511343,21.8226960066454,-8.67640018374703));
#37539=CARTESIAN_POINT('Ctrl Pts',(-20.825412967101,21.8293721310754,-8.67591740191258));
#37540=CARTESIAN_POINT('Ctrl Pts',(-20.8190196150783,21.8395505492243,-8.67518166370546));
#37541=CARTESIAN_POINT('Ctrl Pts',(-20.8168361135681,21.8430415891038,-8.67492937227818));
#37542=CARTESIAN_POINT('Ctrl Pts',(-20.8130596050866,21.8491053887934,-8.67449124392545));
#37543=CARTESIAN_POINT('Ctrl Pts',(-20.8114635163459,21.8516762312068,-8.67430552118253));
#37544=CARTESIAN_POINT('Ctrl Pts',(-20.8081528405154,21.8570255811424,-8.67391913113606));
#37545=CARTESIAN_POINT('Ctrl Pts',(-20.8064388508895,21.8598044528305,-8.67371844207044));
#37546=CARTESIAN_POINT('Ctrl Pts',(-20.8022705686145,21.8665854820809,-8.67322879453893));
#37547=CARTESIAN_POINT('Ctrl Pts',(-20.7998207978715,21.8705903988286,-8.67293967001375));
#37548=CARTESIAN_POINT('Ctrl Pts',(-20.7905727563062,21.885783698563,-8.67184306086649));
#37549=CARTESIAN_POINT('Ctrl Pts',(-20.7838340048356,21.8970079988815,-8.67103339671671));
#37550=CARTESIAN_POINT('Ctrl Pts',(-20.7752603920573,21.9114877085041,-8.66998943357831));
#37551=CARTESIAN_POINT('Ctrl Pts',(-20.773362472356,21.9147057977453,-8.66975744816343));
#37552=CARTESIAN_POINT('Ctrl Pts',(-20.6470196179209,22.1297850367443,-8.65425498018703));
#37553=CARTESIAN_POINT('Ctrl Pts',(-20.5472322348576,22.3551332982661,-8.63805520786541));
#37554=CARTESIAN_POINT('Ctrl Pts',(-20.4260600444248,22.7431450255997,-8.610610334163));
#37555=CARTESIAN_POINT('Ctrl Pts',(-20.3896676012117,22.9000934431723,-8.59964691034359));
#37556=CARTESIAN_POINT('Ctrl Pts',(-20.3547623498811,23.1264556237512,-8.58447374104671));
#37557=CARTESIAN_POINT('Ctrl Pts',(-20.3465150117206,23.1941224702675,-8.58001965843767));
#37558=CARTESIAN_POINT('Ctrl Pts',(-20.3387039558049,23.281103825335,-8.57443927157725));
#37559=CARTESIAN_POINT('Ctrl Pts',(-20.3371592757012,23.3002184327026,-8.57322190673327));
#37560=CARTESIAN_POINT('Ctrl Pts',(-20.3352300448756,23.3270754254476,-8.57152507317009));
#37561=CARTESIAN_POINT('Ctrl Pts',(-20.3347027012597,23.3348067093109,-8.57103819179324));
#37562=CARTESIAN_POINT('Ctrl Pts',(-20.333946910245,23.3465087482352,-8.57030372265756));
#37563=CARTESIAN_POINT('Ctrl Pts',(-20.3336979232892,23.3504780803416,-8.57005502096063));
#37564=CARTESIAN_POINT('Ctrl Pts',(-20.3332537264107,23.3577756133679,-8.569598591661));
#37565=CARTESIAN_POINT('Ctrl Pts',(-20.3330563323339,23.3611036687701,-8.56939074321588));
#37566=CARTESIAN_POINT('Ctrl Pts',(-20.3327463020616,23.3664716871997,-8.56905599391635));
#37567=CARTESIAN_POINT('Ctrl Pts',(-20.3326304414011,23.3685114503679,-8.56892891124367));
#37568=CARTESIAN_POINT('Ctrl Pts',(-20.332411856029,23.3724254476783,-8.56868528475797));
#37569=CARTESIAN_POINT('Ctrl Pts',(-20.3323088298298,23.3742996475945,-8.56856872495959));
#37570=CARTESIAN_POINT('Ctrl Pts',(-20.3320764925918,23.3785946717369,-8.56830183675906));
#37571=CARTESIAN_POINT('Ctrl Pts',(-20.3319482758093,23.3810155493771,-8.5681515710246));
#37572=CARTESIAN_POINT('Ctrl Pts',(-20.3316204993157,23.3873394386585,-8.56775946799688));
#37573=CARTESIAN_POINT('Ctrl Pts',(-20.3314253065119,23.3912426875247,-8.56751787649659));
#37574=CARTESIAN_POINT('Ctrl Pts',(-20.3302409229788,23.4158229306692,-8.56599909490031));
#37575=CARTESIAN_POINT('Ctrl Pts',(-20.3294438425893,23.4365093157595,-8.56473254664616));
#37576=CARTESIAN_POINT('Ctrl Pts',(-20.3185429121785,23.8139015320953,-8.54181511589748));
#37577=CARTESIAN_POINT('Ctrl Pts',(-20.3675489362896,24.1698974975159,-8.5230433003129));
#37578=CARTESIAN_POINT('Ctrl Pts',(-20.5140220449611,24.6390657404455,-8.49482237236206));
#37579=CARTESIAN_POINT('Ctrl Pts',(-20.5621006297161,24.7648104456572,-8.48691579698403));
#37580=CARTESIAN_POINT('Ctrl Pts',(-20.6222434830932,24.8967259915526,-8.47809196986474));
#37581=CARTESIAN_POINT('Ctrl Pts',(-20.6266449914798,24.9062564820922,-8.47745145180394));
#37582=CARTESIAN_POINT('Ctrl Pts',(-20.6330521925172,24.919953639674,-8.47652647867717));
#37583=CARTESIAN_POINT('Ctrl Pts',(-20.6350204434143,24.9241378308387,-8.47624332168835));
#37584=CARTESIAN_POINT('Ctrl Pts',(-20.6384569330991,24.9314026322919,-8.47575064549745));
#37585=CARTESIAN_POINT('Ctrl Pts',(-20.6399210762166,24.9344851810315,-8.47554126885818));
#37586=CARTESIAN_POINT('Ctrl Pts',(-20.6427492535757,24.9404151908375,-8.4751378495098));
#37587=CARTESIAN_POINT('Ctrl Pts',(-20.6441125822772,24.9432629858655,-8.47494383154049));
#37588=CARTESIAN_POINT('Ctrl Pts',(-20.6473395078644,24.9499782078909,-8.47448566046984));
#37589=CARTESIAN_POINT('Ctrl Pts',(-20.6492066487092,24.9538439170566,-8.47422138395562));
#37590=CARTESIAN_POINT('Ctrl Pts',(-20.6557160464583,24.9672524307703,-8.47330289073489));
#37591=CARTESIAN_POINT('Ctrl Pts',(-20.6603976715419,24.9767759494027,-8.47264729926198));
#37592=CARTESIAN_POINT('Ctrl Pts',(-20.7173638708062,25.0912271931706,-8.46472924671945));
#37593=CARTESIAN_POINT('Ctrl Pts',(-20.7752828837738,25.193237254939,-8.45726761195228));
#37594=CARTESIAN_POINT('Ctrl Pts',(-20.9532991613371,25.4704036605692,-8.43579394209326));
#37595=CARTESIAN_POINT('Ctrl Pts',(-21.0853186879591,25.6371710089734,-8.42139094525753));
#37596=CARTESIAN_POINT('Ctrl Pts',(-21.307130334386,25.8667108106903,-8.39981710513638));
#37597=CARTESIAN_POINT('Ctrl Pts',(-21.3853093310627,25.9399386835752,-8.39262118884812));
#37598=CARTESIAN_POINT('Ctrl Pts',(-21.5171575050814,26.0516451680143,-8.38128579137249));
#37599=CARTESIAN_POINT('Ctrl Pts',(-21.5686159624712,26.0926054699292,-8.37704142669657));
#37600=CARTESIAN_POINT('Ctrl Pts',(-21.6269998832273,26.1362276889279,-8.37245287315672));
#37601=CARTESIAN_POINT('Ctrl Pts',(-21.632718198057,26.1404707358687,-8.37200580361167));
#37602=CARTESIAN_POINT('Ctrl Pts',(-21.6414613784863,26.1469134419703,-8.37132587728777));
#37603=CARTESIAN_POINT('Ctrl Pts',(-21.6444760429572,26.1491268119993,-8.37109209300309));
#37604=CARTESIAN_POINT('Ctrl Pts',(-21.6494178719409,26.152741885631,-8.37070994024614));
#37605=CARTESIAN_POINT('Ctrl Pts',(-21.6513427398438,26.1541467007375,-8.37056135755736));
#37606=CARTESIAN_POINT('Ctrl Pts',(-21.6549895370837,26.1568020272018,-8.37028036656029));
#37607=CARTESIAN_POINT('Ctrl Pts',(-21.6567111488156,26.158052969354,-8.37014792828654));
#37608=CARTESIAN_POINT('Ctrl Pts',(-21.65991505099,26.1603761146527,-8.36990186237836));
#37609=CARTESIAN_POINT('Ctrl Pts',(-21.6613970114198,26.1614487581109,-8.36978820408598));
#37610=CARTESIAN_POINT('Ctrl Pts',(-21.664400019948,26.1636184424435,-8.3695582120069));
#37611=CARTESIAN_POINT('Ctrl Pts',(-21.665921106489,26.1647154133497,-8.36944188313231));
#37612=CARTESIAN_POINT('Ctrl Pts',(-21.6702401852203,26.1678245014663,-8.36911204151877));
#37613=CARTESIAN_POINT('Ctrl Pts',(-21.6730404594887,26.1698334668937,-8.36889874852059));
#37614=CARTESIAN_POINT('Ctrl Pts',(-21.6848447517796,26.1782734232808,-8.36800196147861));
#37615=CARTESIAN_POINT('Ctrl Pts',(-21.6938787745485,26.18466261256,-8.36732133145051));
#37616=CARTESIAN_POINT('Ctrl Pts',(-21.8217959020194,26.2741455027789,-8.35776127910911));
#37617=CARTESIAN_POINT('Ctrl Pts',(-21.9461104232022,26.34915831371,-8.3494057343621));
#37618=CARTESIAN_POINT('Ctrl Pts',(-22.0750360458934,26.4155367902838,-8.34120882940695));
#37619=CARTESIAN_POINT('Origin',(-23.5502525316942,23.5502525316942,-77.3107734492734));
#37620=CARTESIAN_POINT('',(-22.075035924178,26.4155367276176,-6.84592209196326));
#37621=CARTESIAN_POINT('',(-22.075036226743,26.4155368833958,-7.0956801988874));
#37622=CARTESIAN_POINT('',(-22.0750360153461,26.4155367745563,-77.3107734492734));
#37623=CARTESIAN_POINT('Ctrl Pts',(-22.075035924178,26.4155367276176,-6.84592209196326));
#37624=CARTESIAN_POINT('Ctrl Pts',(-22.0197506382596,26.3870726150335,-6.84940421266326));
#37625=CARTESIAN_POINT('Ctrl Pts',(-21.9652843228088,26.3570059330645,-6.85289943478171));
#37626=CARTESIAN_POINT('Ctrl Pts',(-21.8038988509854,26.2617172186274,-6.86352482352683));
#37627=CARTESIAN_POINT('Ctrl Pts',(-21.6999020120603,26.1918410910454,-6.87074395872825));
#37628=CARTESIAN_POINT('Ctrl Pts',(-21.572290617936,26.0948579079331,-6.88027526220047));
#37629=CARTESIAN_POINT('Ctrl Pts',(-21.5446917621018,26.0731626981938,-6.88237931436025));
#37630=CARTESIAN_POINT('Ctrl Pts',(-21.5007550814826,26.0374479098907,-6.88580194001471));
#37631=CARTESIAN_POINT('Ctrl Pts',(-21.4841932801137,26.0237075609599,-6.88710931998957));
#37632=CARTESIAN_POINT('Ctrl Pts',(-21.4643247682997,26.0068850468856,-6.888699210864));
#37633=CARTESIAN_POINT('Ctrl Pts',(-21.4608850527187,26.0039602335748,-6.88897524716701));
#37634=CARTESIAN_POINT('Ctrl Pts',(-21.4542504303379,25.9982947030201,-6.88950920555597));
#37635=CARTESIAN_POINT('Ctrl Pts',(-21.4510547227587,25.9955549342969,-6.88976708820377));
#37636=CARTESIAN_POINT('Ctrl Pts',(-21.4455620125885,25.9908271791084,-6.8902115255778));
#37637=CARTESIAN_POINT('Ctrl Pts',(-21.4432624306481,25.9888421865571,-6.89039795599639));
#37638=CARTESIAN_POINT('Ctrl Pts',(-21.4385269923097,25.9847428710865,-6.89078261380928));
#37639=CARTESIAN_POINT('Ctrl Pts',(-21.4360914972207,25.982628137245,-6.8909808581898));
#37640=CARTESIAN_POINT('Ctrl Pts',(-21.4295321007336,25.9769153366405,-6.89151588988145));
#37641=CARTESIAN_POINT('Ctrl Pts',(-21.4254141969134,25.9733104273415,-6.89185296248503));
#37642=CARTESIAN_POINT('Ctrl Pts',(-21.4102843447907,25.9599971731114,-6.89309581957962));
#37643=CARTESIAN_POINT('Ctrl Pts',(-21.399329716625,25.9502242210989,-6.89400431104689));
#37644=CARTESIAN_POINT('Ctrl Pts',(-21.2139024053876,25.7825096665218,-6.90953118559948));
#37645=CARTESIAN_POINT('Ctrl Pts',(-21.0572171822121,25.6060335685424,-6.92499416384261));
#37646=CARTESIAN_POINT('Ctrl Pts',(-20.8157582651171,25.2654413734203,-6.95313835147831));
#37647=CARTESIAN_POINT('Ctrl Pts',(-20.7231559656683,25.1080907292221,-6.96558853688841));
#37648=CARTESIAN_POINT('Ctrl Pts',(-20.6183177297916,24.8894688417338,-6.98158933334656));
#37649=CARTESIAN_POINT('Ctrl Pts',(-20.5938104608102,24.8344617404839,-6.98551108119075));
#37650=CARTESIAN_POINT('Ctrl Pts',(-20.5603612115512,24.7533425272335,-6.99111226674759));
#37651=CARTESIAN_POINT('Ctrl Pts',(-20.5501914478024,24.7277538103183,-6.99285326781846));
#37652=CARTESIAN_POINT('Ctrl Pts',(-20.5387792108028,24.6979307657937,-6.99484990377457));
#37653=CARTESIAN_POINT('Ctrl Pts',(-20.537216340677,24.6938214205829,-6.99512431197436));
#37654=CARTESIAN_POINT('Ctrl Pts',(-20.5348451523088,24.6875481110061,-6.99554212578306));
#37655=CARTESIAN_POINT('Ctrl Pts',(-20.5340307513058,24.6853864753176,-6.99568589634604));
#37656=CARTESIAN_POINT('Ctrl Pts',(-20.5326255826229,24.6816445967516,-6.99593442365807));
#37657=CARTESIAN_POINT('Ctrl Pts',(-20.5320337327216,24.6800647684011,-6.9960392458678));
#37658=CARTESIAN_POINT('Ctrl Pts',(-20.5308020361722,24.6767691187852,-6.99625769101337));
#37659=CARTESIAN_POINT('Ctrl Pts',(-20.530162413194,24.6750532216286,-6.99637130018789));
#37660=CARTESIAN_POINT('Ctrl Pts',(-20.5283994701698,24.6703114830802,-6.99668490570288));
#37661=CARTESIAN_POINT('Ctrl Pts',(-20.5272792287174,24.6672844872493,-6.99688471620227));
#37662=CARTESIAN_POINT('Ctrl Pts',(-20.5229148609401,24.6554369128365,-6.99766527596204));
#37663=CARTESIAN_POINT('Ctrl Pts',(-20.5197047355893,24.6466037298956,-6.99824400337414));
#37664=CARTESIAN_POINT('Ctrl Pts',(-20.4664739988406,24.4981103754237,-7.00792072266327));
#37665=CARTESIAN_POINT('Ctrl Pts',(-20.426109069612,24.355153085545,-7.01646644584718));
#37666=CARTESIAN_POINT('Ctrl Pts',(-20.3557668695526,24.0187701365367,-7.03588540385704));
#37667=CARTESIAN_POINT('Ctrl Pts',(-20.3332521300111,23.824400750828,-7.04661858973753));
#37668=CARTESIAN_POINT('Ctrl Pts',(-20.3266296876275,23.5540997883859,-7.06201081572699));
#37669=CARTESIAN_POINT('Ctrl Pts',(-20.3274156543961,23.4789750112605,-7.06633481668244));
#37670=CARTESIAN_POINT('Ctrl Pts',(-20.3347504468316,23.3175715008311,-7.07579181989363));
#37671=CARTESIAN_POINT('Ctrl Pts',(-20.3421501523385,23.2313933673544,-7.08094463815676));
#37672=CARTESIAN_POINT('Ctrl Pts',(-20.3542178895786,23.1360382679982,-7.08679761800651));
#37673=CARTESIAN_POINT('Ctrl Pts',(-20.3554738983943,23.12645969213,-7.08738725065456));
#37674=CARTESIAN_POINT('Ctrl Pts',(-20.3573806062749,23.1124091225686,-7.08825469845875));
#37675=CARTESIAN_POINT('Ctrl Pts',(-20.3579976824625,23.1079325567065,-7.08853144814527));
#37676=CARTESIAN_POINT('Ctrl Pts',(-20.3590948388877,23.1000951504755,-7.08901663786526));
#37677=CARTESIAN_POINT('Ctrl Pts',(-20.3595708193274,23.0967337355577,-7.08922494762439));
#37678=CARTESIAN_POINT('Ctrl Pts',(-20.3605035622708,23.0902207768709,-7.08962898023459));
#37679=CARTESIAN_POINT('Ctrl Pts',(-20.3609596864279,23.0870691442607,-7.08982468261714));
#37680=CARTESIAN_POINT('Ctrl Pts',(-20.3620568822459,23.0795664300672,-7.09029102334248));
#37681=CARTESIAN_POINT('Ctrl Pts',(-20.3627021898156,23.0752159824504,-7.09056179591816));
#37682=CARTESIAN_POINT('Ctrl Pts',(-20.365026545223,23.059763956866,-7.09152483864947));
#37683=CARTESIAN_POINT('Ctrl Pts',(-20.3667546862896,23.0486699461733,-7.09221866646543));
#37684=CARTESIAN_POINT('Ctrl Pts',(-20.3928278715281,22.8868547251071,-7.10237429446663));
#37685=CARTESIAN_POINT('Ctrl Pts',(-20.427791235932,22.7380640149529,-7.11217798675893));
#37686=CARTESIAN_POINT('Ctrl Pts',(-20.5252808423197,22.4249029218801,-7.13383252295159));
#37687=CARTESIAN_POINT('Ctrl Pts',(-20.5909763216272,22.2620207263261,-7.14574006749728));
#37688=CARTESIAN_POINT('Ctrl Pts',(-20.7474093510081,21.950153773769,-7.16932237688817));
#37689=CARTESIAN_POINT('Ctrl Pts',(-20.8376517130569,21.8015219036287,-7.18095570685641));
#37690=CARTESIAN_POINT('Ctrl Pts',(-20.945575906127,21.6523887903515,-7.19254352937989));
#37691=CARTESIAN_POINT('Ctrl Pts',(-20.9517532577081,21.6439396940987,-7.19319967725875));
#37692=CARTESIAN_POINT('Ctrl Pts',(-20.9598976667474,21.632913296235,-7.1940553426875));
#37693=CARTESIAN_POINT('Ctrl Pts',(-20.961827514737,21.6303087819983,-7.19425741046668));
#37694=CARTESIAN_POINT('Ctrl Pts',(-20.9649856065937,21.6260600516107,-7.19458696040033));
#37695=CARTESIAN_POINT('Ctrl Pts',(-20.966211491198,21.6244140972671,-7.19471460755793));
#37696=CARTESIAN_POINT('Ctrl Pts',(-20.9685669067823,21.6212578574159,-7.19495933987909));
#37697=CARTESIAN_POINT('Ctrl Pts',(-20.9696961878354,21.619747396903,-7.19507644167272));
#37698=CARTESIAN_POINT('Ctrl Pts',(-20.9722944729898,21.6162784357642,-7.1953453406027));
#37699=CARTESIAN_POINT('Ctrl Pts',(-20.973764386886,21.6143206124558,-7.19549707343382));
#37700=CARTESIAN_POINT('Ctrl Pts',(-20.9784303462376,21.6081206052783,-7.19597749288437));
#37701=CARTESIAN_POINT('Ctrl Pts',(-20.9816346698303,21.6038846184055,-7.19630559873236));
#37702=CARTESIAN_POINT('Ctrl Pts',(-21.0088082724573,21.5681461859778,-7.19907288303556));
#37703=CARTESIAN_POINT('Ctrl Pts',(-21.0333469272029,21.5370781687739,-7.20147261345067));
#37704=CARTESIAN_POINT('Ctrl Pts',(-21.0632559300916,21.5006128508458,-7.20429272162335));
#37705=CARTESIAN_POINT('Ctrl Pts',(-21.0680794030325,21.494774125299,-7.20474437797953));
#37706=CARTESIAN_POINT('Ctrl Pts',(-21.0737292604161,21.4879839661316,-7.20526983213132));
#37707=CARTESIAN_POINT('Ctrl Pts',(-21.0745356326535,21.4870160000518,-7.20534474259972));
#37708=CARTESIAN_POINT('Ctrl Pts',(-21.0799257114599,21.4805534800953,-7.20584490777962));
#37709=CARTESIAN_POINT('Ctrl Pts',(-21.0845271753434,21.475073688391,-7.20626917733858));
#37710=CARTESIAN_POINT('Ctrl Pts',(-21.0916158313022,21.4666888147799,-7.20691870115627));
#37711=CARTESIAN_POINT('Ctrl Pts',(-21.094089979903,21.4637727914657,-7.20714464888504));
#37712=CARTESIAN_POINT('Ctrl Pts',(-21.1010885294476,21.455554023175,-7.20778167580901));
#37713=CARTESIAN_POINT('Ctrl Pts',(-21.1056249756417,21.4502615162066,-7.20819212348645));
#37714=CARTESIAN_POINT('Ctrl Pts',(-21.1180648996286,21.4358432460453,-7.20931106403037));
#37715=CARTESIAN_POINT('Ctrl Pts',(-21.1260026016387,21.426747036419,-7.21001782580518));
#37716=CARTESIAN_POINT('Ctrl Pts',(-21.16087804168,21.3872319505114,-7.21309287327705));
#37717=CARTESIAN_POINT('Ctrl Pts',(-21.1883393786652,21.3572785318332,-7.21543633550219));
#37718=CARTESIAN_POINT('Ctrl Pts',(-21.3861382269197,21.1495567426904,-7.23184310489584));
#37719=CARTESIAN_POINT('Ctrl Pts',(-21.5757884018109,20.99130110841,-7.24522923172906));
#37720=CARTESIAN_POINT('Ctrl Pts',(-21.8911457996345,20.784271763947,-7.26681328629581));
#37721=CARTESIAN_POINT('Ctrl Pts',(-22.0049463669217,20.7191207183738,-7.27447409707262));
#37722=CARTESIAN_POINT('Ctrl Pts',(-22.1411842022026,20.651790240033,-7.28366306122662));
#37723=CARTESIAN_POINT('Ctrl Pts',(-22.1600715920662,20.6426841083983,-7.28493717098252));
#37724=CARTESIAN_POINT('Ctrl Pts',(-22.1845685552583,20.6311667026796,-7.28659039846189));
#37725=CARTESIAN_POINT('Ctrl Pts',(-22.1900982878482,20.6285860153399,-7.28696362944073));
#37726=CARTESIAN_POINT('Ctrl Pts',(-22.1990140955313,20.6244558679939,-7.28756549057098));
#37727=CARTESIAN_POINT('Ctrl Pts',(-22.2023956031186,20.6228965354769,-7.28779377891341));
#37728=CARTESIAN_POINT('Ctrl Pts',(-22.2088368209808,20.6199397893123,-7.28822867175003));
#37729=CARTESIAN_POINT('Ctrl Pts',(-22.2118960333682,20.618541297557,-7.28843523867168));
#37730=CARTESIAN_POINT('Ctrl Pts',(-22.2188691111407,20.6153668060595,-7.288906123826));
#37731=CARTESIAN_POINT('Ctrl Pts',(-22.2227843451248,20.6135938439303,-7.28917054632108));
#37732=CARTESIAN_POINT('Ctrl Pts',(-22.234710283656,20.6082220629274,-7.2899760866223));
#37733=CARTESIAN_POINT('Ctrl Pts',(-22.2427321127085,20.6046481731605,-7.29051806040932));
#37734=CARTESIAN_POINT('Ctrl Pts',(-22.3001249174809,20.5793591385182,-7.29439677051276));
#37735=CARTESIAN_POINT('Ctrl Pts',(-22.3500170202423,20.5588547392091,-7.29777467380651));
#37736=CARTESIAN_POINT('Ctrl Pts',(-22.4140850643546,20.5343852073421,-7.30212364495926));
#37737=CARTESIAN_POINT('Ctrl Pts',(-22.427807655864,20.5292510882263,-7.30305577531793));
#37738=CARTESIAN_POINT('Ctrl Pts',(-22.4541202511102,20.5196106208432,-7.30484435547272));
#37739=CARTESIAN_POINT('Ctrl Pts',(-22.4667042585437,20.5150886976141,-7.30570028841363));
#37740=CARTESIAN_POINT('Ctrl Pts',(-22.6214451007938,20.460569273658,-7.31623211236412));
#37741=CARTESIAN_POINT('Ctrl Pts',(-22.7668943240279,20.4205295562629,-7.32621457925477));
#37742=CARTESIAN_POINT('Ctrl Pts',(-23.18050251441,20.3373143667379,-7.35460461532516));
#37743=CARTESIAN_POINT('Ctrl Pts',(-23.4521131899202,20.3175949923935,-7.3733196068634));
#37744=CARTESIAN_POINT('Ctrl Pts',(-23.7309523673661,20.3325625793388,-7.39092232678801));
#37745=CARTESIAN_POINT('Ctrl Pts',(-23.7389079372943,20.3330192170007,-7.3914231132945));
#37746=CARTESIAN_POINT('Ctrl Pts',(-23.7527091742675,20.3338627559439,-7.39228928236897));
#37747=CARTESIAN_POINT('Ctrl Pts',(-23.7585555888035,20.3342360952689,-7.39265539792252));
#37748=CARTESIAN_POINT('Ctrl Pts',(-23.7669648089511,20.3347961171837,-7.39318080944741));
#37749=CARTESIAN_POINT('Ctrl Pts',(-23.7695284161657,20.3349699233796,-7.39334082516806));
#37750=CARTESIAN_POINT('Ctrl Pts',(-23.7739949365616,20.3352781091137,-7.39361933608096));
#37751=CARTESIAN_POINT('Ctrl Pts',(-23.775897941036,20.3354111124483,-7.39373790937933));
#37752=CARTESIAN_POINT('Ctrl Pts',(-23.7795585595508,20.3356702239663,-7.39396582441047));
#37753=CARTESIAN_POINT('Ctrl Pts',(-23.7813161848357,20.3357960837386,-7.39407518015229));
#37754=CARTESIAN_POINT('Ctrl Pts',(-23.7854773149363,20.3360974838674,-7.39433389793387));
#37755=CARTESIAN_POINT('Ctrl Pts',(-23.7878807319196,20.3362742790192,-7.3944831887201));
#37756=CARTESIAN_POINT('Ctrl Pts',(-23.795041475257,20.3368090988884,-7.39492757054652));
#37757=CARTESIAN_POINT('Ctrl Pts',(-23.7997982342611,20.3371749936078,-7.39522221948764));
#37758=CARTESIAN_POINT('Ctrl Pts',(-23.8436990209247,20.3406499646627,-7.39793667612935));
#37759=CARTESIAN_POINT('Ctrl Pts',(-23.8827861173088,20.3444638244165,-7.40031753622912));
#37760=CARTESIAN_POINT('Ctrl Pts',(-23.9271533944665,20.3496131593299,-7.40298896122832));
#37761=CARTESIAN_POINT('Ctrl Pts',(-23.9325093924793,20.3502484152217,-7.40331093826421));
#37762=CARTESIAN_POINT('Ctrl Pts',(-23.9425168420203,20.3514608470295,-7.40391161523707));
#37763=CARTESIAN_POINT('Ctrl Pts',(-23.9471686688015,20.3520347292997,-7.40419045865739));
#37764=CARTESIAN_POINT('Ctrl Pts',(-24.2425503414586,20.3891294865829,-7.42187368644489));
#37765=CARTESIAN_POINT('Ctrl Pts',(-24.5269783353454,20.4651222169242,-7.43760761054507));
#37766=CARTESIAN_POINT('Ctrl Pts',(-24.9486833558827,20.6420776723167,-7.46358547699101));
#37767=CARTESIAN_POINT('Ctrl Pts',(-25.095022855106,20.7170983133602,-7.47313919013141));
#37768=CARTESIAN_POINT('Ctrl Pts',(-25.2460882058468,20.8097364834987,-7.4839058316975));
#37769=CARTESIAN_POINT('Ctrl Pts',(-25.2571382063596,20.8166051275862,-7.48469876807435));
#37770=CARTESIAN_POINT('Ctrl Pts',(-25.2724533744258,20.8262540486807,-7.48580540277979));
#37771=CARTESIAN_POINT('Ctrl Pts',(-25.2767541071204,20.8289778693815,-7.48611700589174));
#37772=CARTESIAN_POINT('Ctrl Pts',(-25.2840026889409,20.8335927773749,-7.48664362388413));
#37773=CARTESIAN_POINT('Ctrl Pts',(-25.2869539519705,20.8354785070013,-7.48685843900778));
#37774=CARTESIAN_POINT('Ctrl Pts',(-25.2927871866065,20.83921909678,-7.48728382543547));
#37775=CARTESIAN_POINT('Ctrl Pts',(-25.2956692852238,20.8410737511152,-7.48749438886363));
#37776=CARTESIAN_POINT('Ctrl Pts',(-25.3020141427269,20.8451710466387,-7.48795879574178));
#37777=CARTESIAN_POINT('Ctrl Pts',(-25.3054755612075,20.8474157443358,-7.48821271598116));
#37778=CARTESIAN_POINT('Ctrl Pts',(-25.3175450081941,20.8552756312968,-7.48910007805005));
#37779=CARTESIAN_POINT('Ctrl Pts',(-25.3261304092142,20.860925301442,-7.48973481326279));
#37780=CARTESIAN_POINT('Ctrl Pts',(-25.413565981602,20.9190640163075,-7.49623552414669));
#37781=CARTESIAN_POINT('Ctrl Pts',(-25.4900851824079,20.9749591011713,-7.50223060793621));
#37782=CARTESIAN_POINT('Ctrl Pts',(-25.7356449412205,21.1714929827473,-7.52254726398655));
#37783=CARTESIAN_POINT('Ctrl Pts',(-25.8927392268272,21.326029592222,-7.53740209862361));
#37784=CARTESIAN_POINT('Ctrl Pts',(-26.1492131399061,21.6358815829431,-7.56461858375501));
#37785=CARTESIAN_POINT('Ctrl Pts',(-26.2534282644208,21.7860899306891,-7.57690935315236));
#37786=CARTESIAN_POINT('Ctrl Pts',(-26.352307292686,21.9581281661657,-7.58946062933366));
#37787=CARTESIAN_POINT('Ctrl Pts',(-26.3601361930593,21.9719861684285,-7.59046139373923));
#37788=CARTESIAN_POINT('Ctrl Pts',(-26.3696845813405,21.9891841240345,-7.59169018059009));
#37789=CARTESIAN_POINT('Ctrl Pts',(-26.3715011413099,21.9924695111648,-7.59192432955634));
#37790=CARTESIAN_POINT('Ctrl Pts',(-26.374350000288,21.9976432177906,-7.59229212133506));
#37791=CARTESIAN_POINT('Ctrl Pts',(-26.3753861483857,21.9995293966235,-7.59242601162495));
#37792=CARTESIAN_POINT('Ctrl Pts',(-26.3773174125475,22.0030533830525,-7.59267579449355));
#37793=CARTESIAN_POINT('Ctrl Pts',(-26.378212989173,22.0046909195042,-7.59279171630674));
#37794=CARTESIAN_POINT('Ctrl Pts',(-26.380217959043,22.0083645270797,-7.593051441398));
#37795=CARTESIAN_POINT('Ctrl Pts',(-26.3813265753743,22.0104010135094,-7.59319519412834));
#37796=CARTESIAN_POINT('Ctrl Pts',(-26.3841342640669,22.0155719132131,-7.59355962845327));
#37797=CARTESIAN_POINT('Ctrl Pts',(-26.3858303396969,22.0187079620325,-7.59378011783683));
#37798=CARTESIAN_POINT('Ctrl Pts',(-26.3950859172378,22.0358896307477,-7.5949852484635));
#37799=CARTESIAN_POINT('Ctrl Pts',(-26.4025464417509,22.0499887340122,-7.59596365069495));
#37800=CARTESIAN_POINT('Ctrl Pts',(-26.5529329359238,22.3393702831933,-7.61584297323554));
#37801=CARTESIAN_POINT('Ctrl Pts',(-26.6555090180112,22.6338560405513,-7.63246398170144));
#37802=CARTESIAN_POINT('Ctrl Pts',(-26.7399041983485,23.0703783247074,-7.6575939504278));
#37803=CARTESIAN_POINT('Ctrl Pts',(-26.7571283042137,23.2036992391386,-7.66531158182004));
#37804=CARTESIAN_POINT('Ctrl Pts',(-26.7696547453009,23.3932105825505,-7.67659269883225));
#37805=CARTESIAN_POINT('Ctrl Pts',(-26.7718858166746,23.4488070625984,-7.67993861777374));
#37806=CARTESIAN_POINT('Ctrl Pts',(-26.7727925374772,23.5125726428198,-7.68382669574348));
#37807=CARTESIAN_POINT('Ctrl Pts',(-26.7728774518515,23.5207146752901,-7.68432409111798));
#37808=CARTESIAN_POINT('Ctrl Pts',(-26.7729591778445,23.5330244982713,-7.68507754346163));
#37809=CARTESIAN_POINT('Ctrl Pts',(-26.772978762445,23.5371921469856,-7.68533288522144));
#37810=CARTESIAN_POINT('Ctrl Pts',(-26.7729986293156,23.5443919324392,-7.6857744360295));
#37811=CARTESIAN_POINT('Ctrl Pts',(-26.7730027168634,23.5474240604204,-7.68596052537403));
#37812=CARTESIAN_POINT('Ctrl Pts',(-26.7730022913777,23.554157356275,-7.68637406427218));
#37813=CARTESIAN_POINT('Ctrl Pts',(-26.7729956815624,23.5578585155528,-7.68660157939536));
#37814=CARTESIAN_POINT('Ctrl Pts',(-26.7729616393149,23.5675611686293,-7.68719854520762));
#37815=CARTESIAN_POINT('Ctrl Pts',(-26.7729238183149,23.5735625909949,-7.68756832155159));
#37816=CARTESIAN_POINT('Ctrl Pts',(-26.7726832764717,23.6000088397494,-7.68920017633913));
#37817=CARTESIAN_POINT('Ctrl Pts',(-26.7723027654457,23.6204512157058,-7.69046782381564));
#37818=CARTESIAN_POINT('Ctrl Pts',(-26.7682127307511,23.765823822046,-7.69952853735467));
#37819=CARTESIAN_POINT('Ctrl Pts',(-26.7574333737421,23.8904334371617,-7.70754346589177));
#37820=CARTESIAN_POINT('Ctrl Pts',(-26.6994066306839,24.2894063658884,-7.73401941320084));
#37821=CARTESIAN_POINT('Ctrl Pts',(-26.6238915515564,24.5583370477323,-7.75323741828679));
#37822=CARTESIAN_POINT('Ctrl Pts',(-26.4786668372663,24.8989532675592,-7.77775052409668));
#37823=CARTESIAN_POINT('Ctrl Pts',(-26.438915609643,24.9821161406006,-7.78373663547824));
#37824=CARTESIAN_POINT('Ctrl Pts',(-26.3926238417019,25.0691615020145,-7.7899174289953));
#37825=CARTESIAN_POINT('Ctrl Pts',(-26.3895796813747,25.0748444321249,-7.79032055367208));
#37826=CARTESIAN_POINT('Ctrl Pts',(-26.3853393278583,25.0827037013147,-7.79087746267443));
#37827=CARTESIAN_POINT('Ctrl Pts',(-26.3841576677842,25.0848878006752,-7.79103216427989));
#37828=CARTESIAN_POINT('Ctrl Pts',(-26.3821239833831,25.0886363645064,-7.79129756535256));
#37829=CARTESIAN_POINT('Ctrl Pts',(-26.38127318656,25.0902014878961,-7.79140834339378));
#37830=CARTESIAN_POINT('Ctrl Pts',(-26.37951470566,25.0934300017869,-7.79163678357562));
#37831=CARTESIAN_POINT('Ctrl Pts',(-26.3786068540261,25.0950932939077,-7.79175443400751));
#37832=CARTESIAN_POINT('Ctrl Pts',(-26.3764747507924,25.0989913811621,-7.79203006913802));
#37833=CARTESIAN_POINT('Ctrl Pts',(-26.375249311568,25.1012255325506,-7.79218797732003));
#37834=CARTESIAN_POINT('Ctrl Pts',(-26.3712725304487,25.1084554248686,-7.79269876347109));
#37835=CARTESIAN_POINT('Ctrl Pts',(-26.3685105568399,25.1134453523507,-7.7930509614482));
#37836=CARTESIAN_POINT('Ctrl Pts',(-26.2978424483562,25.2403220009214,-7.80199824231367));
#37837=CARTESIAN_POINT('Ctrl Pts',(-26.2220948805304,25.3576968327753,-7.81009165701611));
#37838=CARTESIAN_POINT('Ctrl Pts',(-25.9473056772875,25.7282780764366,-7.83627406680274));
#37839=CARTESIAN_POINT('Ctrl Pts',(-25.7180348489133,25.9565739906241,-7.85366426335849));
#37840=CARTESIAN_POINT('Ctrl Pts',(-25.4532069504515,26.1512002860662,-7.87321721883335));
#37841=CARTESIAN_POINT('Ctrl Pts',(-25.4476592596371,26.1552501225843,-7.8736265016008));
#37842=CARTESIAN_POINT('Ctrl Pts',(-25.4056992213984,26.1856759698745,-7.87671984819572));
#37843=CARTESIAN_POINT('Ctrl Pts',(-25.3687528844549,26.2113040670552,-7.87943082517805));
#37844=CARTESIAN_POINT('Ctrl Pts',(-25.3250612315886,26.2402762097737,-7.88262669192885));
#37845=CARTESIAN_POINT('Ctrl Pts',(-25.3188243091784,26.2443808093116,-7.88308266007551));
#37846=CARTESIAN_POINT('Ctrl Pts',(-25.3088535872105,26.2508931275467,-7.88381124397058));
#37847=CARTESIAN_POINT('Ctrl Pts',(-25.3051289491521,26.2533148801365,-7.88408333344342));
#37848=CARTESIAN_POINT('Ctrl Pts',(-25.2985490993852,26.2575737540745,-7.8845638665275));
#37849=CARTESIAN_POINT('Ctrl Pts',(-25.2956959639203,26.2594140836341,-7.88477218986558));
#37850=CARTESIAN_POINT('Ctrl Pts',(-25.2897937799584,26.2632079166924,-7.8852030529357));
#37851=CARTESIAN_POINT('Ctrl Pts',(-25.2867443376308,26.2651607959174,-7.88542561554537));
#37852=CARTESIAN_POINT('Ctrl Pts',(-25.2789348527636,26.2701434914903,-7.88599546805452));
#37853=CARTESIAN_POINT('Ctrl Pts',(-25.2741701472862,26.273165944633,-7.88634303111829));
#37854=CARTESIAN_POINT('Ctrl Pts',(-25.2550594874822,26.2852183730295,-7.88773662985761));
#37855=CARTESIAN_POINT('Ctrl Pts',(-25.2406505271045,26.2941474839875,-7.88878639194285));
#37856=CARTESIAN_POINT('Ctrl Pts',(-25.0548172088165,26.4072875156468,-7.90231438686564));
#37857=CARTESIAN_POINT('Ctrl Pts',(-24.8741291155528,26.4953650136986,-7.91539267488797));
#37858=CARTESIAN_POINT('Ctrl Pts',(-24.5447992712856,26.6194397566855,-7.93897908384512));
#37859=CARTESIAN_POINT('Ctrl Pts',(-24.3995563021428,26.6627619006147,-7.9492910574008));
#37860=CARTESIAN_POINT('Ctrl Pts',(-24.1116559232222,26.7269749093367,-7.96913804888836));
#37861=CARTESIAN_POINT('Ctrl Pts',(-23.9695460862155,26.7488370239252,-7.97866132521248));
#37862=CARTESIAN_POINT('Ctrl Pts',(-23.8172415832172,26.7619373784979,-7.98827349681488));
#37863=CARTESIAN_POINT('Ctrl Pts',(-23.8080445648108,26.7626886760308,-7.98885162159681));
#37864=CARTESIAN_POINT('Ctrl Pts',(-23.7956501934097,26.7636475919997,-7.98962750126572));
#37865=CARTESIAN_POINT('Ctrl Pts',(-23.7924556900058,26.7638899499927,-7.98982718615744));
#37866=CARTESIAN_POINT('Ctrl Pts',(-23.7874394195505,26.7642629981604,-7.99014028838149));
#37867=CARTESIAN_POINT('Ctrl Pts',(-23.785617904823,26.7643969029845,-7.99025388740391));
#37868=CARTESIAN_POINT('Ctrl Pts',(-23.7821124283426,26.7646516047907,-7.99047232271217));
#37869=CARTESIAN_POINT('Ctrl Pts',(-23.7804284966404,26.7647726261987,-7.99057717087911));
#37870=CARTESIAN_POINT('Ctrl Pts',(-23.7764301239966,26.7650568247182,-7.99082593146917));
#37871=CARTESIAN_POINT('Ctrl Pts',(-23.7741156036194,26.7652188255789,-7.99096977650383));
#37872=CARTESIAN_POINT('Ctrl Pts',(-23.7676471865481,26.7656645522312,-7.99137135684123));
#37873=CARTESIAN_POINT('Ctrl Pts',(-23.763492893043,26.7659427292301,-7.99162877910082));
#37874=CARTESIAN_POINT('Ctrl Pts',(-23.7539584901334,26.766562607997,-7.99221848180003));
#37875=CARTESIAN_POINT('Ctrl Pts',(-23.7485780214928,26.7668988637463,-7.99255046027932));
#37876=CARTESIAN_POINT('Ctrl Pts',(-23.6130730692217,26.7750260443758,-8.0008915455931));
#37877=CARTESIAN_POINT('Ctrl Pts',(-23.4825772420055,26.7749292501573,-8.00846945790495));
#37878=CARTESIAN_POINT('Ctrl Pts',(-23.1124961815171,26.7521696128154,-8.02955546359413));
#37879=CARTESIAN_POINT('Ctrl Pts',(-22.8749682800439,26.7106164944346,-8.04265843381471));
#37880=CARTESIAN_POINT('Ctrl Pts',(-22.6064156240064,26.6319476654169,-8.05872055546388));
#37881=CARTESIAN_POINT('Ctrl Pts',(-22.5687747460608,26.6201668962918,-8.06099980100116));
#37882=CARTESIAN_POINT('Ctrl Pts',(-22.4400182187364,26.577258860684,-8.06890834115567));
#37883=CARTESIAN_POINT('Ctrl Pts',(-22.3500939693104,26.5427438278393,-8.07462874202298));
#37884=CARTESIAN_POINT('Ctrl Pts',(-22.2525197660991,26.5001865929291,-8.08110846909325));
#37885=CARTESIAN_POINT('Ctrl Pts',(-22.2432035391128,26.4960706224428,-8.08172993158481));
#37886=CARTESIAN_POINT('Ctrl Pts',(-22.2300920101339,26.4902034205509,-8.08260856349652));
#37887=CARTESIAN_POINT('Ctrl Pts',(-22.2262802964774,26.4884888311914,-8.08286447258066));
#37888=CARTESIAN_POINT('Ctrl Pts',(-22.2196210801126,26.4854777856802,-8.0833123966375));
#37889=CARTESIAN_POINT('Ctrl Pts',(-22.216772103348,26.4841845858986,-8.08350429921969));
#37890=CARTESIAN_POINT('Ctrl Pts',(-22.2107986401567,26.4814626297133,-8.08390723045006));
#37891=CARTESIAN_POINT('Ctrl Pts',(-22.2076745481897,26.4800330225075,-8.08411828826566));
#37892=CARTESIAN_POINT('Ctrl Pts',(-22.2002336828003,26.4766136276573,-8.08462176163667));
#37893=CARTESIAN_POINT('Ctrl Pts',(-22.1959190229425,26.4746192841759,-8.08491433448232));
#37894=CARTESIAN_POINT('Ctrl Pts',(-22.1816604714197,26.4679903019738,-8.08588328568245));
#37895=CARTESIAN_POINT('Ctrl Pts',(-22.171735915897,26.4633144704031,-8.08656109076988));
#37896=CARTESIAN_POINT('Ctrl Pts',(-22.1483337541556,26.4521424585935,-8.08816743889533));
#37897=CARTESIAN_POINT('Ctrl Pts',(-22.1348772185798,26.445602962558,-8.08909748247897));
#37898=CARTESIAN_POINT('Ctrl Pts',(-22.1059249527286,26.4312829118854,-8.09111248113288));
#37899=CARTESIAN_POINT('Ctrl Pts',(-22.0904475042375,26.4234715138296,-8.09219839320965));
#37900=CARTESIAN_POINT('Ctrl Pts',(-22.0750359919087,26.4155367624894,-8.09328852648195));
#37901=CARTESIAN_POINT('Ctrl Pts',(-22.0750360458934,26.4155367902838,-8.34120882940695));
#37902=CARTESIAN_POINT('Ctrl Pts',(-22.1027733724074,26.4298175937409,-8.33944533023278));
#37903=CARTESIAN_POINT('Ctrl Pts',(-22.1307241352365,26.4436987562337,-8.33768934506599));
#37904=CARTESIAN_POINT('Ctrl Pts',(-22.3476372887855,26.5475223062275,-8.3241934062341));
#37905=CARTESIAN_POINT('Ctrl Pts',(-22.5447352738616,26.6192655287509,-8.31265322975392));
#37906=CARTESIAN_POINT('Ctrl Pts',(-22.8253182995639,26.6914405061735,-8.29590793569271));
#37907=CARTESIAN_POINT('Ctrl Pts',(-22.9039606430498,26.7085585341609,-8.29118666463588));
#37908=CARTESIAN_POINT('Ctrl Pts',(-23.0232776285371,26.7298871220935,-8.28393417183107));
#37909=CARTESIAN_POINT('Ctrl Pts',(-23.063529386419,26.7362969482822,-8.2814726218952));
#37910=CARTESIAN_POINT('Ctrl Pts',(-23.111325765456,26.7429813364168,-8.27852870352594));
#37911=CARTESIAN_POINT('Ctrl Pts',(-23.1187645719593,26.7439951740693,-8.27806992833723));
#37912=CARTESIAN_POINT('Ctrl Pts',(-23.1302055508545,26.7455137679747,-8.27736338577484));
#37913=CARTESIAN_POINT('Ctrl Pts',(-23.1342052763479,26.746037023063,-8.27711620448954));
#37914=CARTESIAN_POINT('Ctrl Pts',(-23.1414896408188,26.7469760767165,-8.27666570870248));
#37915=CARTESIAN_POINT('Ctrl Pts',(-23.1447739628976,26.7473943262309,-8.27646247207792));
#37916=CARTESIAN_POINT('Ctrl Pts',(-23.1514181899543,26.7482300478159,-8.27605107607443));
#37917=CARTESIAN_POINT('Ctrl Pts',(-23.1547781194514,26.7486472876449,-8.27584290962085));
#37918=CARTESIAN_POINT('Ctrl Pts',(-23.1643643270776,26.7498223773121,-8.27524862485351));
#37919=CARTESIAN_POINT('Ctrl Pts',(-23.170592143216,26.7505673430807,-8.27486209960974));
#37920=CARTESIAN_POINT('Ctrl Pts',(-23.1972255750654,26.7536743739525,-8.27320720374329));
#37921=CARTESIAN_POINT('Ctrl Pts',(-23.2176509900816,26.7558594499879,-8.27193325524694));
#37922=CARTESIAN_POINT('Ctrl Pts',(-23.5899597744425,26.7920918109801,-8.24862094955779));
#37923=CARTESIAN_POINT('Ctrl Pts',(-23.9449984266275,26.7681926273704,-8.2245088086386));
#37924=CARTESIAN_POINT('Ctrl Pts',(-24.4257627108239,26.6549847105705,-8.19131576487943));
#37925=CARTESIAN_POINT('Ctrl Pts',(-24.5603639068937,26.613839598801,-8.1820141438776));
#37926=CARTESIAN_POINT('Ctrl Pts',(-24.6964988782546,26.5622720290513,-8.17288020746082));
#37927=CARTESIAN_POINT('Ctrl Pts',(-24.7011309094968,26.5605051954651,-8.17256976572695));
#37928=CARTESIAN_POINT('Ctrl Pts',(-24.708454681879,26.5576922536549,-8.17207948617992));
#37929=CARTESIAN_POINT('Ctrl Pts',(-24.7111491018783,26.5566532128094,-8.17189923318364));
#37930=CARTESIAN_POINT('Ctrl Pts',(-24.7162421479843,26.5546813294385,-8.1715587495781));
#37931=CARTESIAN_POINT('Ctrl Pts',(-24.7186410579687,26.5537492335058,-8.1713984744974));
#37932=CARTESIAN_POINT('Ctrl Pts',(-24.722785731101,26.552133104656,-8.17112173553792));
#37933=CARTESIAN_POINT('Ctrl Pts',(-24.7245320161185,26.5514504209651,-8.1710051897376));
#37934=CARTESIAN_POINT('Ctrl Pts',(-24.7279114709179,26.5501258731141,-8.1707797518536));
#37935=CARTESIAN_POINT('Ctrl Pts',(-24.7295447098551,26.5494842000154,-8.17067084832795));
#37936=CARTESIAN_POINT('Ctrl Pts',(-24.7333928010328,26.5479687181692,-8.17041436896415));
#37937=CARTESIAN_POINT('Ctrl Pts',(-24.7356072142842,26.5470937867713,-8.17026686142423));
#37938=CARTESIAN_POINT('Ctrl Pts',(-24.7421502952598,26.544500179238,-8.16983125760568));
#37939=CARTESIAN_POINT('Ctrl Pts',(-24.7464762330029,26.5427745634737,-8.16954357930158));
#37940=CARTESIAN_POINT('Ctrl Pts',(-24.7843097420465,26.5275876363343,-8.16703029531971));
#37941=CARTESIAN_POINT('Ctrl Pts',(-24.817594308191,26.5135727326101,-8.16483757924104));
#37942=CARTESIAN_POINT('Ctrl Pts',(-24.8555208779295,26.4968472759093,-8.16235252470389));
#37943=CARTESIAN_POINT('Ctrl Pts',(-24.8603984751865,26.4946817887547,-8.16203318907669));
#37944=CARTESIAN_POINT('Ctrl Pts',(-24.867854026195,26.491349583959,-8.16154543728902));
#37945=CARTESIAN_POINT('Ctrl Pts',(-24.8704358360506,26.4901915807496,-8.16137659855134));
#37946=CARTESIAN_POINT('Ctrl Pts',(-24.8752382587369,26.4880299779789,-8.16106265973373));
#37947=CARTESIAN_POINT('Ctrl Pts',(-24.8774592624939,26.4870272582532,-8.1609175177101));
#37948=CARTESIAN_POINT('Ctrl Pts',(-24.8809398237862,26.4854511294757,-8.16069013448838));
#37949=CARTESIAN_POINT('Ctrl Pts',(-24.8822001484765,26.4848794285781,-8.16060781266769));
#37950=CARTESIAN_POINT('Ctrl Pts',(-24.8859878549434,26.4831583292754,-8.16036044999131));
#37951=CARTESIAN_POINT('Ctrl Pts',(-24.8885141261842,26.4820064736332,-8.16019552446968));
#37952=CARTESIAN_POINT('Ctrl Pts',(-24.8973672231942,26.477956068701,-8.15961774651599));
#37953=CARTESIAN_POINT('Ctrl Pts',(-24.9036861878226,26.4750402731629,-8.15920569221256));
#37954=CARTESIAN_POINT('Ctrl Pts',(-24.9144233997497,26.4700434926081,-8.15850602393743));
#37955=CARTESIAN_POINT('Ctrl Pts',(-24.918846425972,26.4679729031039,-8.15821795035371));
#37956=CARTESIAN_POINT('Ctrl Pts',(-25.0411406844188,26.4103829649947,-8.15025639976279));
#37957=CARTESIAN_POINT('Ctrl Pts',(-25.1555524840572,26.3477713371421,-8.14289564430797));
#37958=CARTESIAN_POINT('Ctrl Pts',(-25.3455622371713,26.2282823326868,-8.13031624572085));
#37959=CARTESIAN_POINT('Ctrl Pts',(-25.4230228408465,26.1746976060524,-8.12507691590084));
#37960=CARTESIAN_POINT('Ctrl Pts',(-25.5849292193896,26.0518733257388,-8.11367516110724));
#37961=CARTESIAN_POINT('Ctrl Pts',(-25.6684245288969,25.9815815925956,-8.10750465582291));
#37962=CARTESIAN_POINT('Ctrl Pts',(-25.805707866571,25.853559662363,-8.0966435515795));
#37963=CARTESIAN_POINT('Ctrl Pts',(-25.8612377607683,25.7978397593696,-8.09202481811507));
#37964=CARTESIAN_POINT('Ctrl Pts',(-25.9417814537768,25.710877141744,-8.08492938055546));
#37965=CARTESIAN_POINT('Ctrl Pts',(-25.9683446958331,25.6811066698828,-8.08251918563339));
#37966=CARTESIAN_POINT('Ctrl Pts',(-25.9992115915905,25.645192333475,-8.07963038798964));
#37967=CARTESIAN_POINT('Ctrl Pts',(-26.0040559142288,25.6395160881938,-8.07917436229542));
#37968=CARTESIAN_POINT('Ctrl Pts',(-26.0114821111363,25.6307531236746,-8.0784711697199));
#37969=CARTESIAN_POINT('Ctrl Pts',(-26.0140780140244,25.6276782820735,-8.07822458018652));
#37970=CARTESIAN_POINT('Ctrl Pts',(-26.018798952275,25.6220650452144,-8.07777469842422));
#37971=CARTESIAN_POINT('Ctrl Pts',(-26.0209258513901,25.6195282187291,-8.07757148296681));
#37972=CARTESIAN_POINT('Ctrl Pts',(-26.025224120011,25.6143854502174,-8.07715972043681));
#37973=CARTESIAN_POINT('Ctrl Pts',(-26.0273952912495,25.6117793486308,-8.07695116563234));
#37974=CARTESIAN_POINT('Ctrl Pts',(-26.0335893812555,25.6043205409911,-8.07635456976985));
#37975=CARTESIAN_POINT('Ctrl Pts',(-26.037602166206,25.599459473415,-8.07596611668119));
#37976=CARTESIAN_POINT('Ctrl Pts',(-26.0547973185164,25.5785044304303,-8.07429309605373));
#37977=CARTESIAN_POINT('Ctrl Pts',(-26.0678377071591,25.5622950773466,-8.07300279876892));
#37978=CARTESIAN_POINT('Ctrl Pts',(-26.3015945846025,25.2659019857957,-8.04947427850338));
#37979=CARTESIAN_POINT('Ctrl Pts',(-26.4744011216352,24.9511636370712,-8.02511985781829));
#37980=CARTESIAN_POINT('Ctrl Pts',(-26.6181705880062,24.5403062515305,-7.99588921291723));
#37981=CARTESIAN_POINT('Ctrl Pts',(-26.6414632008705,24.4649905915381,-7.99064555231686));
#37982=CARTESIAN_POINT('Ctrl Pts',(-26.6714024691744,24.3539028460264,-7.98314355246942));
#37983=CARTESIAN_POINT('Ctrl Pts',(-26.6802421271728,24.318755057165,-7.9808033403347));
#37984=CARTESIAN_POINT('Ctrl Pts',(-26.6945041685765,24.2577117809356,-7.97680501887104));
#37985=CARTESIAN_POINT('Ctrl Pts',(-26.7002039223492,24.2318853453675,-7.97513365473354));
#37986=CARTESIAN_POINT('Ctrl Pts',(-26.7064731853699,24.2017184082633,-7.9732072616159));
#37987=CARTESIAN_POINT('Ctrl Pts',(-26.7073523713557,24.197444316228,-7.97293493059533));
#37988=CARTESIAN_POINT('Ctrl Pts',(-26.7086785687674,24.1909301015901,-7.97252079842349));
#37989=CARTESIAN_POINT('Ctrl Pts',(-26.7091318793789,24.1886912891946,-7.97237863660468));
#37990=CARTESIAN_POINT('Ctrl Pts',(-26.7099153032998,24.1848008506082,-7.97213189192108));
#37991=CARTESIAN_POINT('Ctrl Pts',(-26.7102465013438,24.1831494515242,-7.9720272465312));
#37992=CARTESIAN_POINT('Ctrl Pts',(-26.7109376417045,24.1796892632944,-7.97180817507932));
#37993=CARTESIAN_POINT('Ctrl Pts',(-26.7112973249707,24.1778804299507,-7.97169376431004));
#37994=CARTESIAN_POINT('Ctrl Pts',(-26.7121819299133,24.1734117357072,-7.97141138397589));
#37995=CARTESIAN_POINT('Ctrl Pts',(-26.7127050494356,24.1707515131819,-7.97124351829627));
#37996=CARTESIAN_POINT('Ctrl Pts',(-26.714749014116,24.1602876008245,-7.970584139389));
#37997=CARTESIAN_POINT('Ctrl Pts',(-26.7162443534286,24.1524788684637,-7.97009407839292));
#37998=CARTESIAN_POINT('Ctrl Pts',(-26.7412387479329,24.0192906178819,-7.96176832121097));
#37999=CARTESIAN_POINT('Ctrl Pts',(-26.7573053855183,23.8926127085319,-7.95434433055858));
#38000=CARTESIAN_POINT('Ctrl Pts',(-26.7705420263195,23.6946878378139,-7.94305245767932));
#38001=CARTESIAN_POINT('Ctrl Pts',(-26.7729373045662,23.6239369448992,-7.93907683542844));
#38002=CARTESIAN_POINT('Ctrl Pts',(-26.7730990812615,23.4447935440941,-7.9290490962535));
#38003=CARTESIAN_POINT('Ctrl Pts',(-26.7677307660088,23.3364887109567,-7.92302063020588));
#38004=CARTESIAN_POINT('Ctrl Pts',(-26.7372827827145,23.0328840570655,-7.90582579634958));
#38005=CARTESIAN_POINT('Ctrl Pts',(-26.6997648651561,22.8393472354877,-7.89448984911841));
#38006=CARTESIAN_POINT('Ctrl Pts',(-26.6414829389786,22.6389036114505,-7.8818003566766));
#38007=CARTESIAN_POINT('Ctrl Pts',(-26.6380595015311,22.6273709595411,-7.88106697024858));
#38008=CARTESIAN_POINT('Ctrl Pts',(-26.6332583336872,22.6115229093171,-7.88005453761369));
#38009=CARTESIAN_POINT('Ctrl Pts',(-26.6319359257343,22.6071907428344,-7.87977730601066));
#38010=CARTESIAN_POINT('Ctrl Pts',(-26.6296579015256,22.59978396452,-7.8793024971622));
#38011=CARTESIAN_POINT('Ctrl Pts',(-26.6287067999128,22.5967079615213,-7.87910506838526));
#38012=CARTESIAN_POINT('Ctrl Pts',(-26.6268486629605,22.5907302284907,-7.87872092206963));
#38013=CARTESIAN_POINT('Ctrl Pts',(-26.625942127876,22.5878283460515,-7.87853422118583));
#38014=CARTESIAN_POINT('Ctrl Pts',(-26.6237659208148,22.5808966316009,-7.87808772728309));
#38015=CARTESIAN_POINT('Ctrl Pts',(-26.6224924299964,22.5768680130396,-7.87782780876598));
#38016=CARTESIAN_POINT('Ctrl Pts',(-26.6186571450679,22.5648178053215,-7.8770490815737));
#38017=CARTESIAN_POINT('Ctrl Pts',(-26.6160718448458,22.5568037870361,-7.8765294985445));
#38018=CARTESIAN_POINT('Ctrl Pts',(-26.5934589102471,22.4876362501003,-7.87203031425878));
#38019=CARTESIAN_POINT('Ctrl Pts',(-26.5716364968613,22.4270889667166,-7.86799155454542));
#38020=CARTESIAN_POINT('Ctrl Pts',(-26.5113142837528,22.274232058428,-7.85752532548827));
#38021=CARTESIAN_POINT('Ctrl Pts',(-26.4703058205187,22.1829923266424,-7.85101822124881));
#38022=CARTESIAN_POINT('Ctrl Pts',(-26.2882392541963,21.8236101232849,-7.82435943025246));
#38023=CARTESIAN_POINT('Ctrl Pts',(-26.1139600849322,21.5740819773777,-7.80328546753548));
#38024=CARTESIAN_POINT('Ctrl Pts',(-25.8761468421943,21.3190113921817,-7.78073651511226));
#38025=CARTESIAN_POINT('Ctrl Pts',(-25.8441538442873,21.2861326855571,-7.77781130067336));
#38026=CARTESIAN_POINT('Ctrl Pts',(-25.807917245031,21.2504498367488,-7.77462689539191));
#38027=CARTESIAN_POINT('Ctrl Pts',(-25.8043585222615,21.2469617168805,-7.77431550393104));
#38028=CARTESIAN_POINT('Ctrl Pts',(-25.7990283903411,21.241761516157,-7.77385113449051));
#38029=CARTESIAN_POINT('Ctrl Pts',(-25.797263106283,21.2400432102181,-7.77369767010195));
#38030=CARTESIAN_POINT('Ctrl Pts',(-25.7942216271018,21.2370894556621,-7.77343383011151));
#38031=CARTESIAN_POINT('Ctrl Pts',(-25.7929463811705,21.2358530383009,-7.77332337800509));
#38032=CARTESIAN_POINT('Ctrl Pts',(-25.7903062185187,21.233297494212,-7.77309506396332));
#38033=CARTESIAN_POINT('Ctrl Pts',(-25.7889411609392,21.2319785213852,-7.77297721452394));
#38034=CARTESIAN_POINT('Ctrl Pts',(-25.7857271012518,21.2288784553251,-7.77270019634926));
#38035=CARTESIAN_POINT('Ctrl Pts',(-25.7838771297016,21.2270983592676,-7.77254110637254));
#38036=CARTESIAN_POINT('Ctrl Pts',(-25.7778350806992,21.2212984139785,-7.77202267395487));
#38037=CARTESIAN_POINT('Ctrl Pts',(-25.773634232397,21.2172876564159,-7.77166404028104));
#38038=CARTESIAN_POINT('Ctrl Pts',(-25.6700462915769,21.1189210485666,-7.76286442144645));
#38039=CARTESIAN_POINT('Ctrl Pts',(-25.5647370106838,21.0309745787545,-7.75490694471442));
#38040=CARTESIAN_POINT('Ctrl Pts',(-25.1642005083345,20.7377065102569,-7.72671156060172));
#38041=CARTESIAN_POINT('Ctrl Pts',(-24.8408384203233,20.5754185193488,-7.70736257398968));
#38042=CARTESIAN_POINT('Ctrl Pts',(-24.4778610643212,20.4638183409789,-7.68439760225522));
#38043=CARTESIAN_POINT('Ctrl Pts',(-24.4583085677271,20.4580093638461,-7.68315817725747));
#38044=CARTESIAN_POINT('Ctrl Pts',(-24.4326901071784,20.4506621375966,-7.6815307184455));
#38045=CARTESIAN_POINT('Ctrl Pts',(-24.4266726514745,20.4489553097915,-7.68114819685265));
#38046=CARTESIAN_POINT('Ctrl Pts',(-24.4173937443339,20.4463525462855,-7.68055794850676));
#38047=CARTESIAN_POINT('Ctrl Pts',(-24.4141357642512,20.4454442022724,-7.68035062643563));
#38048=CARTESIAN_POINT('Ctrl Pts',(-24.4077191618574,20.4436660973486,-7.67994215296765));
#38049=CARTESIAN_POINT('Ctrl Pts',(-24.4045606306618,20.4427960206846,-7.67974101213375));
#38050=CARTESIAN_POINT('Ctrl Pts',(-24.3975983563228,20.440889548928,-7.67929748032723));
#38051=CARTESIAN_POINT('Ctrl Pts',(-24.3937940313525,20.4398553153815,-7.67905501937595));
#38052=CARTESIAN_POINT('Ctrl Pts',(-24.3859093580297,20.4377273387596,-7.67855228159195));
#38053=CARTESIAN_POINT('Ctrl Pts',(-24.3818287397242,20.4366346331685,-7.67829197152332));
#38054=CARTESIAN_POINT('Ctrl Pts',(-24.3713901654202,20.4338613821585,-7.67762575300873));
#38055=CARTESIAN_POINT('Ctrl Pts',(-24.3650292151008,20.432192274808,-7.67721947376594));
#38056=CARTESIAN_POINT('Ctrl Pts',(-24.2365118091935,20.3988895475909,-7.66900463091696));
#38057=CARTESIAN_POINT('Ctrl Pts',(-24.1126226464172,20.3744418970721,-7.66096355652652));
#38058=CARTESIAN_POINT('Ctrl Pts',(-23.6777772341081,20.3148751691724,-7.63227785922372));
#38059=CARTESIAN_POINT('Ctrl Pts',(-23.3634531601954,20.3177626822699,-7.61054704511752));
#38060=CARTESIAN_POINT('Ctrl Pts',(-23.026956487317,20.3701494345289,-7.58820916618623));
#38061=CARTESIAN_POINT('Ctrl Pts',(-22.9994712860129,20.3747943637344,-7.58639314134667));
#38062=CARTESIAN_POINT('Ctrl Pts',(-22.9625873822551,20.3815209662901,-7.58397058567214));
#38063=CARTESIAN_POINT('Ctrl Pts',(-22.9531334561969,20.3832888634942,-7.58335093081142));
#38064=CARTESIAN_POINT('Ctrl Pts',(-22.908650358688,20.3918135347791,-7.58044178940181));
#38065=CARTESIAN_POINT('Ctrl Pts',(-22.8737253039417,20.3991096565588,-7.57817669532825));
#38066=CARTESIAN_POINT('Ctrl Pts',(-22.8344004436264,20.4080089243122,-7.57565325381026));
#38067=CARTESIAN_POINT('Ctrl Pts',(-22.8298762199363,20.4090430400775,-7.5753633444375));
#38068=CARTESIAN_POINT('Ctrl Pts',(-22.8230383767599,20.4106215367747,-7.57492581067109));
#38069=CARTESIAN_POINT('Ctrl Pts',(-22.8207231241657,20.4111587046422,-7.57477777384441));
#38070=CARTESIAN_POINT('Ctrl Pts',(-22.8167005900308,20.4120966740617,-7.57452076661325));
#38071=CARTESIAN_POINT('Ctrl Pts',(-22.814993041676,20.4124963078483,-7.57441172858877));
#38072=CARTESIAN_POINT('Ctrl Pts',(-22.8114218868183,20.4133351743791,-7.5741838148974));
#38073=CARTESIAN_POINT('Ctrl Pts',(-22.8095583467037,20.4137746738455,-7.57406495533706));
#38074=CARTESIAN_POINT('Ctrl Pts',(-22.805106415622,20.4148288114091,-7.57378117606285));
#38075=CARTESIAN_POINT('Ctrl Pts',(-22.8025183842176,20.4154449961598,-7.57361634623355));
#38076=CARTESIAN_POINT('Ctrl Pts',(-22.7937686629748,20.4175396704427,-7.57305954378833));
#38077=CARTESIAN_POINT('Ctrl Pts',(-22.7876105209057,20.4190331398793,-7.57266843402244));
#38078=CARTESIAN_POINT('Ctrl Pts',(-22.7729971040031,20.4226228466437,-7.57174207224171));
#38079=CARTESIAN_POINT('Ctrl Pts',(-22.7645457942233,20.4247352347653,-7.57120772814764));
#38080=CARTESIAN_POINT('Ctrl Pts',(-22.6657505800121,20.4498549461405,-7.56497650322715));
#38081=CARTESIAN_POINT('Ctrl Pts',(-22.5764277707128,20.4767402306257,-7.55949147945837));
#38082=CARTESIAN_POINT('Ctrl Pts',(-22.1143153238479,20.6380070601651,-7.53130129787237));
#38083=CARTESIAN_POINT('Ctrl Pts',(-21.7675303923484,20.8363923443027,-7.510320278491));
#38084=CARTESIAN_POINT('Ctrl Pts',(-21.4512084036797,21.1047513549594,-7.48520708112283));
#38085=CARTESIAN_POINT('Ctrl Pts',(-21.4371552115809,21.1168840947281,-7.48407818197906));
#38086=CARTESIAN_POINT('Ctrl Pts',(-21.4186810127926,21.1331144033881,-7.48257620904785));
#38087=CARTESIAN_POINT('Ctrl Pts',(-21.4141653513498,21.1371040843972,-7.482207644042));
#38088=CARTESIAN_POINT('Ctrl Pts',(-21.4071670854613,21.1433222331838,-7.48163420149487));
#38089=CARTESIAN_POINT('Ctrl Pts',(-21.4046766907698,21.1455419456881,-7.48142969205957));
#38090=CARTESIAN_POINT('Ctrl Pts',(-21.3997447499392,21.1499515922087,-7.48102379880451));
#38091=CARTESIAN_POINT('Ctrl Pts',(-21.3973030910476,21.1521413946996,-7.4808224206613));
#38092=CARTESIAN_POINT('Ctrl Pts',(-21.3918772712116,21.1570225080977,-7.48037395518879));
#38093=CARTESIAN_POINT('Ctrl Pts',(-21.3888947964292,21.1597156775789,-7.48012678938378));
#38094=CARTESIAN_POINT('Ctrl Pts',(-21.3827094557098,21.1653220669865,-7.47961283155348));
#38095=CARTESIAN_POINT('Ctrl Pts',(-21.3795074093389,21.1682361754918,-7.47934600202121));
#38096=CARTESIAN_POINT('Ctrl Pts',(-21.3712723405181,21.1757611166437,-7.47865779238412));
#38097=CARTESIAN_POINT('Ctrl Pts',(-21.366248095886,21.1803814852224,-7.47823600581103));
#38098=CARTESIAN_POINT('Ctrl Pts',(-21.2264437084075,21.3097698042006,-7.46644576468609));
#38099=CARTESIAN_POINT('Ctrl Pts',(-21.1025845550344,21.4457928625825,-7.45457460958322));
#38100=CARTESIAN_POINT('Ctrl Pts',(-20.8003020252485,21.8407675532035,-7.42145620117746));
#38101=CARTESIAN_POINT('Ctrl Pts',(-20.6470248879265,22.1164345263202,-7.3995784102034));
#38102=CARTESIAN_POINT('Ctrl Pts',(-20.5303172132053,22.4249231191531,-7.37870750556253));
#38103=CARTESIAN_POINT('Ctrl Pts',(-20.5247453215897,22.4399905077765,-7.37769706253502));
#38104=CARTESIAN_POINT('Ctrl Pts',(-20.51807148182,22.4584611501325,-7.37646984976302));
#38105=CARTESIAN_POINT('Ctrl Pts',(-20.516862359323,22.4618250409831,-7.37624681140183));
#38106=CARTESIAN_POINT('Ctrl Pts',(-20.5148771614592,22.4673770474963,-7.37587946408081));
#38107=CARTESIAN_POINT('Ctrl Pts',(-20.5140978536367,22.4695639903065,-7.3757349625728));
#38108=CARTESIAN_POINT('Ctrl Pts',(-20.5126961953752,22.4735108955834,-7.37547453005728));
#38109=CARTESIAN_POINT('Ctrl Pts',(-20.5120730124375,22.4752705522759,-7.37535854927597));
#38110=CARTESIAN_POINT('Ctrl Pts',(-20.5107353484412,22.4790581151543,-7.37510918358271));
#38111=CARTESIAN_POINT('Ctrl Pts',(-20.5100213697326,22.481086189529,-7.3749758292263));
#38112=CARTESIAN_POINT('Ctrl Pts',(-20.5080693629404,22.4866486792233,-7.37461053452757));
#38113=CARTESIAN_POINT('Ctrl Pts',(-20.5068354601497,22.4901845545296,-7.37437884104576));
#38114=CARTESIAN_POINT('Ctrl Pts',(-20.500429236452,22.5086456270193,-7.37317177852662));
#38115=CARTESIAN_POINT('Ctrl Pts',(-20.4953604176021,22.5236068910809,-7.37220249846643));
#38116=CARTESIAN_POINT('Ctrl Pts',(-20.446006030417,22.6728852565413,-7.36261456760133));
#38117=CARTESIAN_POINT('Ctrl Pts',(-20.4104915558757,22.8099611024345,-7.35447612640773));
#38118=CARTESIAN_POINT('Ctrl Pts',(-20.3202263773212,23.2852469436229,-7.32714302270412));
#38119=CARTESIAN_POINT('Ctrl Pts',(-20.3103444437043,23.6295386550922,-7.30856965493013));
#38120=CARTESIAN_POINT('Ctrl Pts',(-20.3574729044258,23.9892218926378,-7.28663275899283));
#38121=CARTESIAN_POINT('Ctrl Pts',(-20.3603229031716,24.0094744641432,-7.28539001900837));
#38122=CARTESIAN_POINT('Ctrl Pts',(-20.3642969379311,24.0358899716173,-7.28375881129066));
#38123=CARTESIAN_POINT('Ctrl Pts',(-20.3652464887885,24.0420789993281,-7.28337588744482));
#38124=CARTESIAN_POINT('Ctrl Pts',(-20.3667369299289,24.0516081184797,-7.28278515471257));
#38125=CARTESIAN_POINT('Ctrl Pts',(-20.3672650577443,24.0549502150887,-7.28257775158426));
#38126=CARTESIAN_POINT('Ctrl Pts',(-20.3683146411837,24.0615250086614,-7.2821693016435));
#38127=CARTESIAN_POINT('Ctrl Pts',(-20.3688357624952,24.0647577554809,-7.28196826568818));
#38128=CARTESIAN_POINT('Ctrl Pts',(-20.3699948404363,24.0718789369338,-7.28152496175955));
#38129=CARTESIAN_POINT('Ctrl Pts',(-20.3706350028136,24.0757670027254,-7.28128262387341));
#38130=CARTESIAN_POINT('Ctrl Pts',(-20.3719756651998,24.0838174655993,-7.2807802237549));
#38131=CARTESIAN_POINT('Ctrl Pts',(-20.3726772147983,24.0879796780882,-7.28052012848436));
#38132=CARTESIAN_POINT('Ctrl Pts',(-20.374491327004,24.0986150698178,-7.27985463426606));
#38133=CARTESIAN_POINT('Ctrl Pts',(-20.3756155013793,24.1050862249402,-7.27944886567115));
#38134=CARTESIAN_POINT('Ctrl Pts',(-20.3985112787847,24.2345346827897,-7.27131481831905));
#38135=CARTESIAN_POINT('Ctrl Pts',(-20.4273904825377,24.3561313698521,-7.26335885976496));
#38136=CARTESIAN_POINT('Ctrl Pts',(-20.5518396320275,24.7712397858069,-7.23504924387579));
#38137=CARTESIAN_POINT('Ctrl Pts',(-20.6823820105249,25.0524390524938,-7.2136390709152));
#38138=CARTESIAN_POINT('Ctrl Pts',(-20.8606112213619,25.3257144778976,-7.19218286367889));
#38139=CARTESIAN_POINT('Ctrl Pts',(-20.8704758257952,25.3405687973587,-7.19101501618376));
#38140=CARTESIAN_POINT('Ctrl Pts',(-20.8875747195906,25.3658586643454,-7.18902500362645));
#38141=CARTESIAN_POINT('Ctrl Pts',(-20.8947482518326,25.3763346189272,-7.18820015798606));
#38142=CARTESIAN_POINT('Ctrl Pts',(-20.9045778682259,25.390508998168,-7.18708369444735));
#38143=CARTESIAN_POINT('Ctrl Pts',(-20.9071800611662,25.3942444522974,-7.18678942712698));
#38144=CARTESIAN_POINT('Ctrl Pts',(-20.9105833375204,25.3991078590964,-7.18640626455059));
#38145=CARTESIAN_POINT('Ctrl Pts',(-20.9113772309816,25.4002408083155,-7.18631700261827));
#38146=CARTESIAN_POINT('Ctrl Pts',(-20.9136496699999,25.403479320753,-7.18606184212426));
#38147=CARTESIAN_POINT('Ctrl Pts',(-20.91513001128,25.4055836300355,-7.18589603628198));
#38148=CARTESIAN_POINT('Ctrl Pts',(-20.9393438542113,25.4399162358462,-7.18319074019616));
#38149=CARTESIAN_POINT('Ctrl Pts',(-20.9626658713115,25.4717281792872,-7.18068244356887));
#38150=CARTESIAN_POINT('Ctrl Pts',(-20.9894618910131,25.5069057140191,-7.17791429256693));
#38151=CARTESIAN_POINT('Ctrl Pts',(-20.9923649640141,25.5106993106473,-7.17761584461479));
#38152=CARTESIAN_POINT('Ctrl Pts',(-20.9967462855692,25.5163983118868,-7.17716762433079));
#38153=CARTESIAN_POINT('Ctrl Pts',(-20.9982182392707,25.518308513712,-7.17701741085929));
#38154=CARTESIAN_POINT('Ctrl Pts',(-21.0007697668526,25.5216120374818,-7.17675767054288));
#38155=CARTESIAN_POINT('Ctrl Pts',(-21.0018483394941,25.5230061256575,-7.17664807254734));
#38156=CARTESIAN_POINT('Ctrl Pts',(-21.0040965053413,25.5259070284073,-7.17642004174227));
#38157=CARTESIAN_POINT('Ctrl Pts',(-21.0052662913075,25.5274136877906,-7.17630162355166));
#38158=CARTESIAN_POINT('Ctrl Pts',(-21.008046555063,25.5309880526312,-7.17602072565351));
#38159=CARTESIAN_POINT('Ctrl Pts',(-21.009658223546,25.5330548398034,-7.17585833106925));
#38160=CARTESIAN_POINT('Ctrl Pts',(-21.015034671403,25.53993222416,-7.17531803470594));
#38161=CARTESIAN_POINT('Ctrl Pts',(-21.0188106364079,25.5447341209768,-7.17494092753518));
#38162=CARTESIAN_POINT('Ctrl Pts',(-21.0277613206181,25.5560503443414,-7.17405247575955));
#38163=CARTESIAN_POINT('Ctrl Pts',(-21.0329476853058,25.5625554634222,-7.17354194281066));
#38164=CARTESIAN_POINT('Ctrl Pts',(-21.2231435446671,25.7992270438193,-7.15497157238212));
#38165=CARTESIAN_POINT('Ctrl Pts',(-21.43892396765,26.0029413827232,-7.13903697806157));
#38166=CARTESIAN_POINT('Ctrl Pts',(-21.8054377756668,26.2642292166013,-7.1137044483494));
#38167=CARTESIAN_POINT('Ctrl Pts',(-21.9376365380647,26.3447954713216,-7.10486479826434));
#38168=CARTESIAN_POINT('Ctrl Pts',(-22.0750362267429,26.4155368833958,-7.0956801988874));
#38169=CARTESIAN_POINT('Origin',(-23.5502525316942,23.5502525316942,-77.3107734492734));
#38170=CARTESIAN_POINT('',(-22.0750360126322,26.415536773159,-5.59931610453398));
#38171=CARTESIAN_POINT('',(-22.0750360153462,26.4155367745563,-5.84297427009708));
#38172=CARTESIAN_POINT('',(-22.0750360153461,26.4155367745563,-77.3107734492734));
#38173=CARTESIAN_POINT('',(-26.7730012642694,23.5472912798725,-6.43954486607156));
#38174=CARTESIAN_POINT('Ctrl Pts',(-22.0750360126322,26.415536773159,-5.59931610453398));
#38175=CARTESIAN_POINT('Ctrl Pts',(-22.063724523342,26.4097129544905,-5.60012170027255));
#38176=CARTESIAN_POINT('Ctrl Pts',(-22.0524467684468,26.4038217657381,-5.60092356050259));
#38177=CARTESIAN_POINT('Ctrl Pts',(-22.035388410705,26.3947819421545,-5.6021340599298));
#38178=CARTESIAN_POINT('Ctrl Pts',(-22.0295828565831,26.391682561278,-5.60254561634457));
#38179=CARTESIAN_POINT('Ctrl Pts',(-22.0215807446687,26.3873789659974,-5.60311226489102));
#38180=CARTESIAN_POINT('Ctrl Pts',(-22.0193760875055,26.3861899691922,-5.60326831651584));
#38181=CARTESIAN_POINT('Ctrl Pts',(-22.0156007797741,26.3841482173037,-5.6035354279953));
#38182=CARTESIAN_POINT('Ctrl Pts',(-22.0140294527887,26.3832967262774,-5.60364656869388));
#38183=CARTESIAN_POINT('Ctrl Pts',(-22.0109627599141,26.3816316054116,-5.60386340928337));
#38184=CARTESIAN_POINT('Ctrl Pts',(-22.0094673343102,26.3808180999374,-5.60396911645944));
#38185=CARTESIAN_POINT('Ctrl Pts',(-22.0058484757369,26.3788457379252,-5.60422484709094));
#38186=CARTESIAN_POINT('Ctrl Pts',(-22.003725696766,26.3776856720766,-5.60437479255021));
#38187=CARTESIAN_POINT('Ctrl Pts',(-21.9972864569809,26.3741573059139,-5.60482945192425));
#38188=CARTESIAN_POINT('Ctrl Pts',(-21.9929740897392,26.3717814892022,-5.60513368482178));
#38189=CARTESIAN_POINT('Ctrl Pts',(-21.9518812703501,26.3490192737425,-5.6080304856339));
#38190=CARTESIAN_POINT('Ctrl Pts',(-21.9154955631361,26.3279235049876,-5.61057821400722));
#38191=CARTESIAN_POINT('Ctrl Pts',(-21.8071402780183,26.262234035031,-5.61814493675557));
#38192=CARTESIAN_POINT('Ctrl Pts',(-21.7365008852309,26.2155088454694,-5.62305057754278));
#38193=CARTESIAN_POINT('Ctrl Pts',(-21.4915986841601,26.0392637084911,-5.64026052344134));
#38194=CARTESIAN_POINT('Ctrl Pts',(-21.3286757484282,25.8949988838077,-5.65212942729478));
#38195=CARTESIAN_POINT('Ctrl Pts',(-21.1345504790544,25.684565793705,-5.66839747726744));
#38196=CARTESIAN_POINT('Ctrl Pts',(-21.0892666023558,25.6321884098,-5.67237000093987));
#38197=CARTESIAN_POINT('Ctrl Pts',(-20.9842346285269,25.5024848115661,-5.6820896367509));
#38198=CARTESIAN_POINT('Ctrl Pts',(-20.9262516058788,25.4238253127145,-5.68789078817834));
#38199=CARTESIAN_POINT('Ctrl Pts',(-20.8667487331098,25.3349126754141,-5.69440291406271));
#38200=CARTESIAN_POINT('Ctrl Pts',(-20.8615976667254,25.3271429278105,-5.69497159930759));
#38201=CARTESIAN_POINT('Ctrl Pts',(-20.8539998478598,25.3155738756375,-5.69581783669036));
#38202=CARTESIAN_POINT('Ctrl Pts',(-20.8515272268767,25.3117915495037,-5.69609441788861));
#38203=CARTESIAN_POINT('Ctrl Pts',(-20.8473081291278,25.3053079343158,-5.69656839280282));
#38204=CARTESIAN_POINT('Ctrl Pts',(-20.8455577215627,25.3026092001756,-5.69676563917922));
#38205=CARTESIAN_POINT('Ctrl Pts',(-20.8421603277807,25.2973539671783,-5.69714965953264));
#38206=CARTESIAN_POINT('Ctrl Pts',(-20.8405129137032,25.2947977484659,-5.69733641721698));
#38207=CARTESIAN_POINT('Ctrl Pts',(-20.8365814337363,25.2886784424515,-5.697783412599));
#38208=CARTESIAN_POINT('Ctrl Pts',(-20.8343007682676,25.2851131870638,-5.69804377660317));
#38209=CARTESIAN_POINT('Ctrl Pts',(-20.827763521138,25.2748493366561,-5.6987931428397));
#38210=CARTESIAN_POINT('Ctrl Pts',(-20.8235246748178,25.2681395317649,-5.69928280294182));
#38211=CARTESIAN_POINT('Ctrl Pts',(-20.7903870258501,25.2152532413282,-5.70314062634239));
#38212=CARTESIAN_POINT('Ctrl Pts',(-20.7626399347143,25.1683688426381,-5.70655101200951));
#38213=CARTESIAN_POINT('Ctrl Pts',(-20.6727389245209,25.0072819688946,-5.71824650037768));
#38214=CARTESIAN_POINT('Ctrl Pts',(-20.6163171685644,24.8900418754303,-5.72672830605924));
#38215=CARTESIAN_POINT('Ctrl Pts',(-20.4935755162458,24.5897872262508,-5.7483164924717));
#38216=CARTESIAN_POINT('Ctrl Pts',(-20.4364509153238,24.4035635391301,-5.76160629553261));
#38217=CARTESIAN_POINT('Ctrl Pts',(-20.3752536246944,24.1124974193806,-5.78155445360239));
#38218=CARTESIAN_POINT('Ctrl Pts',(-20.3588974691573,24.0106808575185,-5.78837694683938));
#38219=CARTESIAN_POINT('Ctrl Pts',(-20.3467322294419,23.9018442567204,-5.79539362631764));
#38220=CARTESIAN_POINT('Ctrl Pts',(-20.3460357703165,23.8954394602199,-5.795805526485));
#38221=CARTESIAN_POINT('Ctrl Pts',(-20.3426088837517,23.8630207599918,-5.79788512881315));
#38222=CARTESIAN_POINT('Ctrl Pts',(-20.340175923412,23.8369754166747,-5.79953869060973));
#38223=CARTESIAN_POINT('Ctrl Pts',(-20.3376857283784,23.8062867878733,-5.80146454788215));
#38224=CARTESIAN_POINT('Ctrl Pts',(-20.3373211500304,23.8016703979298,-5.80175364983733));
#38225=CARTESIAN_POINT('Ctrl Pts',(-20.3367849184805,23.7946887907792,-5.80218995257939));
#38226=CARTESIAN_POINT('Ctrl Pts',(-20.3366059256461,23.7923241687189,-5.80233756556574));
#38227=CARTESIAN_POINT('Ctrl Pts',(-20.3362903793652,23.7880935426048,-5.80260137664039));
#38228=CARTESIAN_POINT('Ctrl Pts',(-20.3361528411214,23.7862276197839,-5.80271763038156));
#38229=CARTESIAN_POINT('Ctrl Pts',(-20.3358632126738,23.7822511219033,-5.80296516594238));
#38230=CARTESIAN_POINT('Ctrl Pts',(-20.3357115766012,23.7801405222098,-5.80309642150182));
#38231=CARTESIAN_POINT('Ctrl Pts',(-20.3353132086466,23.7745182321665,-5.80344572604508));
#38232=CARTESIAN_POINT('Ctrl Pts',(-20.3350701508892,23.7710062717047,-5.80366356708278));
#38233=CARTESIAN_POINT('Ctrl Pts',(-20.3339434935503,23.7543304598567,-5.80469629928081));
#38234=CARTESIAN_POINT('Ctrl Pts',(-20.3331349643533,23.7411614148443,-5.80550700483182));
#38235=CARTESIAN_POINT('Ctrl Pts',(-20.3272406890403,23.6344471041889,-5.81203987684769));
#38236=CARTESIAN_POINT('Ctrl Pts',(-20.3261547043276,23.5407157741036,-5.81755050553904));
#38237=CARTESIAN_POINT('Ctrl Pts',(-20.335180784728,23.2589685108632,-5.83378266651929));
#38238=CARTESIAN_POINT('Ctrl Pts',(-20.3576702856288,23.0717553473858,-5.84414029915698));
#38239=CARTESIAN_POINT('Ctrl Pts',(-20.4403388374241,22.6783160947907,-5.8667147990062));
#38240=CARTESIAN_POINT('Ctrl Pts',(-20.5050125597034,22.4739955236306,-5.87895602386481));
#38241=CARTESIAN_POINT('Ctrl Pts',(-20.5946190640516,22.2655264795962,-5.89273967519777));
#38242=CARTESIAN_POINT('Ctrl Pts',(-20.5998817597666,22.2534863522571,-5.89354034775661));
#38243=CARTESIAN_POINT('Ctrl Pts',(-20.6071273374206,22.2371821752148,-5.89463095316069));
#38244=CARTESIAN_POINT('Ctrl Pts',(-20.6090461878465,22.2328896687128,-5.89491868637259));
#38245=CARTESIAN_POINT('Ctrl Pts',(-20.6123141391625,22.2256219279921,-5.89540688198937));
#38246=CARTESIAN_POINT('Ctrl Pts',(-20.6136583869862,22.222644508321,-5.89560717714834));
#38247=CARTESIAN_POINT('Ctrl Pts',(-20.6162562287122,22.2169137115935,-5.8959932628735));
#38248=CARTESIAN_POINT('Ctrl Pts',(-20.6175091774203,22.2141600450138,-5.89617903099987));
#38249=CARTESIAN_POINT('Ctrl Pts',(-20.620474705415,22.2076668292775,-5.89661767558438));
#38250=CARTESIAN_POINT('Ctrl Pts',(-20.6221905668943,22.2039287928653,-5.89687066522584));
#38251=CARTESIAN_POINT('Ctrl Pts',(-20.6271274233568,22.1932278374947,-5.89759625569906));
#38252=CARTESIAN_POINT('Ctrl Pts',(-20.6303661155788,22.1862731568453,-5.89806946860222));
#38253=CARTESIAN_POINT('Ctrl Pts',(-20.6519982108467,22.1402511015888,-5.90121191071184));
#38254=CARTESIAN_POINT('Ctrl Pts',(-20.6711496245791,22.1015467993871,-5.90390740442488));
#38255=CARTESIAN_POINT('Ctrl Pts',(-20.728098030659,21.9920481855956,-5.91169005363148));
#38256=CARTESIAN_POINT('Ctrl Pts',(-20.7677671005214,21.9222691654528,-5.91684185235081));
#38257=CARTESIAN_POINT('Ctrl Pts',(-20.9183734453319,21.6789612794698,-5.93550565588518));
#38258=CARTESIAN_POINT('Ctrl Pts',(-21.0432719840423,21.5146815904178,-5.94946857391438));
#38259=CARTESIAN_POINT('Ctrl Pts',(-21.2846196065572,21.2534137871243,-5.97351840251512));
#38260=CARTESIAN_POINT('Ctrl Pts',(-21.3938335950998,21.1505802439385,-5.98358388905972));
#38261=CARTESIAN_POINT('Ctrl Pts',(-21.5371624265648,21.0333429319211,-5.99547450515909));
#38262=CARTESIAN_POINT('Ctrl Pts',(-21.5648759683189,21.0114248764869,-5.99771730836098));
#38263=CARTESIAN_POINT('Ctrl Pts',(-21.5966219588899,20.987155467447,-6.00021822732889));
#38264=CARTESIAN_POINT('Ctrl Pts',(-21.6003042699486,20.9843529325479,-6.00050729449055));
#38265=CARTESIAN_POINT('Ctrl Pts',(-21.6058842073651,20.9801251002199,-6.00094376853211));
#38266=CARTESIAN_POINT('Ctrl Pts',(-21.6077773730306,20.9786939667895,-6.00109158507234));
#38267=CARTESIAN_POINT('Ctrl Pts',(-21.6110714710975,20.9762095155866,-6.00134831222763));
#38268=CARTESIAN_POINT('Ctrl Pts',(-21.6124716817199,20.9751552496374,-6.00145729011387));
#38269=CARTESIAN_POINT('Ctrl Pts',(-21.6154037770047,20.9729513216398,-6.00168518279387));
#38270=CARTESIAN_POINT('Ctrl Pts',(-21.6169358255962,20.9718018835693,-6.00180408133511));
#38271=CARTESIAN_POINT('Ctrl Pts',(-21.6199914381382,20.9695136275547,-6.00204086807108));
#38272=CARTESIAN_POINT('Ctrl Pts',(-21.6215149892718,20.9683747899856,-6.0021587577056));
#38273=CARTESIAN_POINT('Ctrl Pts',(-21.6268244729824,20.9644133321559,-6.00256899385718));
#38274=CARTESIAN_POINT('Ctrl Pts',(-21.6306156244474,20.9615976671134,-6.00286085150361));
#38275=CARTESIAN_POINT('Ctrl Pts',(-21.6643621075381,20.9366492627511,-6.00544947413248));
#38276=CARTESIAN_POINT('Ctrl Pts',(-21.6946944001577,20.9150278631143,-6.00771112161255));
#38277=CARTESIAN_POINT('Ctrl Pts',(-21.775051020258,20.8598238690149,-6.01355393327951));
#38278=CARTESIAN_POINT('Ctrl Pts',(-21.825655679397,20.8271085018592,-6.01708663232258));
#38279=CARTESIAN_POINT('Ctrl Pts',(-22.0150123232969,20.7120888115148,-6.02988934053061));
#38280=CARTESIAN_POINT('Ctrl Pts',(-22.1589748486629,20.638811515233,-6.03883474407486));
#38281=CARTESIAN_POINT('Ctrl Pts',(-22.5334021454231,20.4823705509512,-6.06152683659764));
#38282=CARTESIAN_POINT('Ctrl Pts',(-22.7689296300542,20.4141093235015,-6.07535300421617));
#38283=CARTESIAN_POINT('Ctrl Pts',(-23.0254904249645,20.3704738189411,-6.09113452621829));
#38284=CARTESIAN_POINT('Ctrl Pts',(-23.0411085526091,20.3679357144448,-6.09209763733198));
#38285=CARTESIAN_POINT('Ctrl Pts',(-23.062323655014,20.3646482172907,-6.0934093610934));
#38286=CARTESIAN_POINT('Ctrl Pts',(-23.0679050204813,20.3637983402095,-6.09375478022829));
#38287=CARTESIAN_POINT('Ctrl Pts',(-23.0767124019181,20.3624809066119,-6.09430037268543));
#38288=CARTESIAN_POINT('Ctrl Pts',(-23.0799369617617,20.3620035682754,-6.09450023532779));
#38289=CARTESIAN_POINT('Ctrl Pts',(-23.0861574309734,20.3610923814813,-6.09488600329405));
#38290=CARTESIAN_POINT('Ctrl Pts',(-23.0891532397423,20.3606578600969,-6.09507188706333));
#38291=CARTESIAN_POINT('Ctrl Pts',(-23.0962361440897,20.3596407210667,-6.09551159565997));
#38292=CARTESIAN_POINT('Ctrl Pts',(-23.1003237485212,20.3590617357452,-6.09576553535798));
#38293=CARTESIAN_POINT('Ctrl Pts',(-23.1087731626088,20.3578814824401,-6.09629082610496));
#38294=CARTESIAN_POINT('Ctrl Pts',(-23.1131351123858,20.357281296172,-6.0965622109116));
#38295=CARTESIAN_POINT('Ctrl Pts',(-23.1371096762377,20.3540325434197,-6.0980549737405));
#38296=CARTESIAN_POINT('Ctrl Pts',(-23.1567447920976,20.351555787205,-6.09928178089781));
#38297=CARTESIAN_POINT('Ctrl Pts',(-23.2903701528085,20.3359493684545,-6.10766082438145));
#38298=CARTESIAN_POINT('Ctrl Pts',(-23.4049555385619,20.3287362512678,-6.11499911898354));
#38299=CARTESIAN_POINT('Ctrl Pts',(-23.6941657212413,20.3259917262129,-6.13391840766884));
#38300=CARTESIAN_POINT('Ctrl Pts',(-23.8684911540879,20.3385112897054,-6.14569976153674));
#38301=CARTESIAN_POINT('Ctrl Pts',(-24.2384028881567,20.3954960500221,-6.17103463608782));
#38302=CARTESIAN_POINT('Ctrl Pts',(-24.4326463636069,20.4442196423082,-6.18454452428901));
#38303=CARTESIAN_POINT('Ctrl Pts',(-24.6321176102573,20.5144954793993,-6.19787402576032));
#38304=CARTESIAN_POINT('Ctrl Pts',(-24.6430703752855,20.5184210556133,-6.19860405301831));
#38305=CARTESIAN_POINT('Ctrl Pts',(-24.6573042499791,20.5236097693767,-6.1995500948583));
#38306=CARTESIAN_POINT('Ctrl Pts',(-24.6606047086928,20.5248190154916,-6.19976926876306));
#38307=CARTESIAN_POINT('Ctrl Pts',(-24.665675975797,20.5266864795396,-6.20010574015303));
#38308=CARTESIAN_POINT('Ctrl Pts',(-24.6674481814717,20.527340853931,-6.20022326769941));
#38309=CARTESIAN_POINT('Ctrl Pts',(-24.6709685207579,20.5286442328724,-6.20045661403557));
#38310=CARTESIAN_POINT('Ctrl Pts',(-24.6727166565766,20.5292931926702,-6.20057243419586));
#38311=CARTESIAN_POINT('Ctrl Pts',(-24.6766109571913,20.5307427193792,-6.20083032261912));
#38312=CARTESIAN_POINT('Ctrl Pts',(-24.6787568271319,20.5315440554394,-6.20097234357785));
#38313=CARTESIAN_POINT('Ctrl Pts',(-24.6831935828207,20.5332062731168,-6.20126581524193));
#38314=CARTESIAN_POINT('Ctrl Pts',(-24.6854843470187,20.5340674781385,-6.2014172464195));
#38315=CARTESIAN_POINT('Ctrl Pts',(-24.6979368805879,20.5387651620218,-6.20223992947922));
#38316=CARTESIAN_POINT('Ctrl Pts',(-24.7080803484192,20.5426504474456,-6.20290827709475));
#38317=CARTESIAN_POINT('Ctrl Pts',(-24.7344815196078,20.5529163343628,-6.20464365123393));
#38318=CARTESIAN_POINT('Ctrl Pts',(-24.7507075798561,20.5593780302172,-6.20570604935727));
#38319=CARTESIAN_POINT('Ctrl Pts',(-24.8016005130155,20.5801260011768,-6.20902754637784));
#38320=CARTESIAN_POINT('Ctrl Pts',(-24.8360722523715,20.5948860095794,-6.21126159755536));
#38321=CARTESIAN_POINT('Ctrl Pts',(-24.9580011324386,20.649630589157,-6.21913398732912));
#38322=CARTESIAN_POINT('Ctrl Pts',(-25.0439221055966,20.6929255204805,-6.22462725559394));
#38323=CARTESIAN_POINT('Ctrl Pts',(-25.1987938595158,20.7798625898991,-6.23465082557216));
#38324=CARTESIAN_POINT('Ctrl Pts',(-25.268268867073,20.822401863889,-6.23919594220282));
#38325=CARTESIAN_POINT('Ctrl Pts',(-25.5543275496574,21.0128222215559,-6.25839756610085));
#38326=CARTESIAN_POINT('Ctrl Pts',(-25.7540132678255,21.1841837558739,-6.27312975266344));
#38327=CARTESIAN_POINT('Ctrl Pts',(-25.9325328898397,21.3797998110134,-6.28918777977869));
#38328=CARTESIAN_POINT('Ctrl Pts',(-25.9343335432908,21.3817778494361,-6.28935007491363));
#38329=CARTESIAN_POINT('Ctrl Pts',(-25.9455147081148,21.3940912477223,-6.29035987219193));
#38330=CARTESIAN_POINT('Ctrl Pts',(-25.9548303431019,21.4044850895927,-6.29121006933741));
#38331=CARTESIAN_POINT('Ctrl Pts',(-25.9676285159456,21.4189525463152,-6.29239061851167));
#38332=CARTESIAN_POINT('Ctrl Pts',(-25.9711689461682,21.4229749309816,-6.29271854318657));
#38333=CARTESIAN_POINT('Ctrl Pts',(-25.9768096314042,21.42941579484,-6.29324315913686));
#38334=CARTESIAN_POINT('Ctrl Pts',(-25.9789163519597,21.4318286197831,-6.29343958054804));
#38335=CARTESIAN_POINT('Ctrl Pts',(-25.9832421302096,21.4367978632578,-6.29384389733176));
#38336=CARTESIAN_POINT('Ctrl Pts',(-25.9854607635615,21.4393546446971,-6.29405180999267));
#38337=CARTESIAN_POINT('Ctrl Pts',(-25.9905904496408,21.4452850107866,-6.29453378858206));
#38338=CARTESIAN_POINT('Ctrl Pts',(-25.993498537112,21.4486611407394,-6.29480797683903));
#38339=CARTESIAN_POINT('Ctrl Pts',(-25.9995612175773,21.4557291717413,-6.29538158684159));
#38340=CARTESIAN_POINT('Ctrl Pts',(-26.0027144844718,21.459422190922,-6.29568106244243));
#38341=CARTESIAN_POINT('Ctrl Pts',(-26.0110943601165,21.4692815086413,-6.29647996562938));
#38342=CARTESIAN_POINT('Ctrl Pts',(-26.0163061113498,21.4754603388099,-6.29698000274442));
#38343=CARTESIAN_POINT('Ctrl Pts',(-26.0577738519428,21.5249997015529,-6.30098415029472));
#38344=CARTESIAN_POINT('Ctrl Pts',(-26.0929047146583,21.5692852378482,-6.30453373693261));
#38345=CARTESIAN_POINT('Ctrl Pts',(-26.2082727622755,21.7228443667021,-6.3167523883879));
#38346=CARTESIAN_POINT('Ctrl Pts',(-26.2827657855241,21.8362351505098,-6.32563382942593));
#38347=CARTESIAN_POINT('Ctrl Pts',(-26.3736137348248,21.9955684839366,-6.33788287018465));
#38348=CARTESIAN_POINT('Ctrl Pts',(-26.3964035121164,22.037693319323,-6.34109979622353));
#38349=CARTESIAN_POINT('Ctrl Pts',(-26.4401216443222,22.1229913843143,-6.34756173858693));
#38350=CARTESIAN_POINT('Ctrl Pts',(-26.4610418595475,22.1661559769787,-6.35080601614751));
#38351=CARTESIAN_POINT('Ctrl Pts',(-26.5682692600392,22.4005907038362,-6.36825539361215));
#38352=CARTESIAN_POINT('Ctrl Pts',(-26.6367132344579,22.5995011482201,-6.38249260988721));
#38353=CARTESIAN_POINT('Ctrl Pts',(-26.6883235926518,22.8162265797965,-6.396550692061));
#38354=CARTESIAN_POINT('Ctrl Pts',(-26.6912376113156,22.8287978729241,-6.39736097356616));
#38355=CARTESIAN_POINT('Ctrl Pts',(-26.6948808735499,22.844955756726,-6.39839550618231));
#38356=CARTESIAN_POINT('Ctrl Pts',(-26.6956795736996,22.8485263223217,-6.3986236840252));
#38357=CARTESIAN_POINT('Ctrl Pts',(-26.6968877156592,22.8539707923373,-6.39897094631893));
#38358=CARTESIAN_POINT('Ctrl Pts',(-26.6973015645529,22.8558436994092,-6.39909028477759));
#38359=CARTESIAN_POINT('Ctrl Pts',(-26.6980740770463,22.8593546427886,-6.39931376911895));
#38360=CARTESIAN_POINT('Ctrl Pts',(-26.6984331330208,22.8609925838192,-6.39941793734522));
#38361=CARTESIAN_POINT('Ctrl Pts',(-26.6992538582189,22.8647505872837,-6.39965672276031));
#38362=CARTESIAN_POINT('Ctrl Pts',(-26.6997146640603,22.8668708322729,-6.39979128935125));
#38363=CARTESIAN_POINT('Ctrl Pts',(-26.7006549725435,22.8712185012591,-6.40006691057121));
#38364=CARTESIAN_POINT('Ctrl Pts',(-26.7011342551285,22.8734459723272,-6.40020795244094));
#38365=CARTESIAN_POINT('Ctrl Pts',(-26.7023419326268,22.8790877538382,-6.40056476235431));
#38366=CARTESIAN_POINT('Ctrl Pts',(-26.7030671448463,22.8825027538046,-6.40078034858068));
#38367=CARTESIAN_POINT('Ctrl Pts',(-26.7051212866385,22.8922535878424,-6.40139480797495));
#38368=CARTESIAN_POINT('Ctrl Pts',(-26.7064366861524,22.8985923013127,-6.40179292063658));
#38369=CARTESIAN_POINT('Ctrl Pts',(-26.7509312414172,23.1163001452387,-6.41542217472304));
#38370=CARTESIAN_POINT('Ctrl Pts',(-26.7728029487694,23.3314996865643,-6.42748399422408));
#38371=CARTESIAN_POINT('Ctrl Pts',(-26.773001172026,23.5472921703334,-6.43954507713563));
#38372=CARTESIAN_POINT('Ctrl Pts',(-26.7730011711998,23.5472912709714,-6.43954502686845));
#38373=CARTESIAN_POINT('Ctrl Pts',(-26.7732230558275,23.7887689553493,-6.45304170831777));
#38374=CARTESIAN_POINT('Ctrl Pts',(-26.7463060136877,24.0294874392209,-6.46649688886903));
#38375=CARTESIAN_POINT('Ctrl Pts',(-26.6820697803317,24.3119354550827,-6.48374203233462));
#38376=CARTESIAN_POINT('Ctrl Pts',(-26.6703299556146,24.3586810346309,-6.48664260123069));
#38377=CARTESIAN_POINT('Ctrl Pts',(-26.655776080884,24.411580349893,-6.48998385616881));
#38378=CARTESIAN_POINT('Ctrl Pts',(-26.6539852996154,24.4180111555374,-6.49039103739883));
#38379=CARTESIAN_POINT('Ctrl Pts',(-26.6510173503438,24.4285425191072,-6.4910595050076));
#38380=CARTESIAN_POINT('Ctrl Pts',(-26.6498519913166,24.4326464075783,-6.49132040669056));
#38381=CARTESIAN_POINT('Ctrl Pts',(-26.6475700316367,24.4406221770286,-6.49182826619843));
#38382=CARTESIAN_POINT('Ctrl Pts',(-26.6464543104562,24.4444943031065,-6.49207519494048));
#38383=CARTESIAN_POINT('Ctrl Pts',(-26.6444906813123,24.4512613749443,-6.49250738781117));
#38384=CARTESIAN_POINT('Ctrl Pts',(-26.6436459638527,24.4541572478825,-6.49269254739924));
#38385=CARTESIAN_POINT('Ctrl Pts',(-26.6418660094643,24.4602275964951,-6.4930811199475));
#38386=CARTESIAN_POINT('Ctrl Pts',(-26.6409299466505,24.4634018245479,-6.49328455976424));
#38387=CARTESIAN_POINT('Ctrl Pts',(-26.6383132212585,24.4722251326235,-6.49385076100227));
#38388=CARTESIAN_POINT('Ctrl Pts',(-26.6366219550606,24.4778710314381,-6.49421386957783));
#38389=CARTESIAN_POINT('Ctrl Pts',(-26.6298254988347,24.5003350626034,-6.49566184684453));
#38390=CARTESIAN_POINT('Ctrl Pts',(-26.6245983262605,24.5171157025802,-6.4967507138592));
#38391=CARTESIAN_POINT('Ctrl Pts',(-26.5361596965184,24.7930577014278,-6.51477785529035));
#38392=CARTESIAN_POINT('Ctrl Pts',(-26.4206005378816,25.0406364163846,-6.53287137644403));
#38393=CARTESIAN_POINT('Ctrl Pts',(-26.2530808927883,25.3059795584539,-6.55410624166824));
#38394=CARTESIAN_POINT('Ctrl Pts',(-26.2301231170608,25.3408256792051,-6.55693208372932));
#38395=CARTESIAN_POINT('Ctrl Pts',(-26.1843397903856,25.4074635120278,-6.56239947988033));
#38396=CARTESIAN_POINT('Ctrl Pts',(-26.1615987168668,25.4393050685869,-6.56504110869971));
#38397=CARTESIAN_POINT('Ctrl Pts',(-26.0782998946827,25.5515586486335,-6.57444253231218));
#38398=CARTESIAN_POINT('Ctrl Pts',(-26.0145572076743,25.6295445760625,-6.58114193440231));
#38399=CARTESIAN_POINT('Ctrl Pts',(-25.9165222236781,25.738631029702,-6.59062696741362));
#38400=CARTESIAN_POINT('Ctrl Pts',(-25.8850500832053,25.7721781934054,-6.59356058400394));
#38401=CARTESIAN_POINT('Ctrl Pts',(-25.8501346087193,25.8078342610322,-6.59668586638776));
#38402=CARTESIAN_POINT('Ctrl Pts',(-25.8473954805612,25.8106213303006,-6.59693020409052));
#38403=CARTESIAN_POINT('Ctrl Pts',(-25.8429284531141,25.8151500350231,-6.59732729717358));
#38404=CARTESIAN_POINT('Ctrl Pts',(-25.8412036326767,25.816894681273,-6.59748029078148));
#38405=CARTESIAN_POINT('Ctrl Pts',(-25.8378614909972,25.8202675269138,-6.59777609575074));
#38406=CARTESIAN_POINT('Ctrl Pts',(-25.8362444202288,25.8218959708893,-6.59791892666539));
#38407=CARTESIAN_POINT('Ctrl Pts',(-25.833310109964,25.8248446126631,-6.59817757390651));
#38408=CARTESIAN_POINT('Ctrl Pts',(-25.8319934681808,25.826165390157,-6.59829343684241));
#38409=CARTESIAN_POINT('Ctrl Pts',(-25.8293426034048,25.8288199690645,-6.59852632064472));
#38410=CARTESIAN_POINT('Ctrl Pts',(-25.8280083610934,25.8301537364171,-6.59864333893968));
#38411=CARTESIAN_POINT('Ctrl Pts',(-25.8241939423418,25.833960106765,-6.59897731736106));
#38412=CARTESIAN_POINT('Ctrl Pts',(-25.8217108958063,25.8364298493745,-6.59919404871169));
#38413=CARTESIAN_POINT('Ctrl Pts',(-25.8110382634302,25.8470107465006,-6.60012273242578));
#38414=CARTESIAN_POINT('Ctrl Pts',(-25.8028090882138,25.8550821113522,-6.60083156192904));
#38415=CARTESIAN_POINT('Ctrl Pts',(-25.6564107619157,25.9971399518233,-6.61331827075779));
#38416=CARTESIAN_POINT('Ctrl Pts',(-25.5065319231081,26.1185507036374,-6.62417822589037));
#38417=CARTESIAN_POINT('Ctrl Pts',(-25.287432125624,26.2656565608257,-6.63895276722549));
#38418=CARTESIAN_POINT('Ctrl Pts',(-25.2268690493698,26.3034632123035,-6.64293159181647));
#38419=CARTESIAN_POINT('Ctrl Pts',(-25.1037968105329,26.374723427399,-6.65089475792966));
#38420=CARTESIAN_POINT('Ctrl Pts',(-25.0413407091383,26.4081873222685,-6.65487662653799));
#38421=CARTESIAN_POINT('Ctrl Pts',(-24.8711861190572,26.4922590682175,-6.66566099626532));
#38422=CARTESIAN_POINT('Ctrl Pts',(-24.7617121414733,26.5390030068505,-6.67253673072892));
#38423=CARTESIAN_POINT('Ctrl Pts',(-24.6179701255674,26.59118190569,-6.68163753340397));
#38424=CARTESIAN_POINT('Ctrl Pts',(-24.5858474294374,26.6022707810536,-6.68367548845767));
#38425=CARTESIAN_POINT('Ctrl Pts',(-24.533612988942,26.6193827331942,-6.68699905541715));
#38426=CARTESIAN_POINT('Ctrl Pts',(-24.5136067364435,26.6257210531457,-6.68827427018309));
#38427=CARTESIAN_POINT('Ctrl Pts',(-24.4892547224055,26.6331752579444,-6.68982965075675));
#38428=CARTESIAN_POINT('Ctrl Pts',(-24.4849663627025,26.6344781563839,-6.69010366968577));
#38429=CARTESIAN_POINT('Ctrl Pts',(-24.4766681380678,26.6369804439564,-6.69063414685645));
#38430=CARTESIAN_POINT('Ctrl Pts',(-24.4726586250458,26.6381809762597,-6.69089056708677));
#38431=CARTESIAN_POINT('Ctrl Pts',(-24.4657381235725,26.6402384380939,-6.69133334013744));
#38432=CARTESIAN_POINT('Ctrl Pts',(-24.4628282355226,26.6410990751779,-6.69151957130211));
#38433=CARTESIAN_POINT('Ctrl Pts',(-24.4568135995572,26.6428687475485,-6.69190462368179));
#38434=CARTESIAN_POINT('Ctrl Pts',(-24.4537086905922,26.6437772199989,-6.69210346308038));
#38435=CARTESIAN_POINT('Ctrl Pts',(-24.4461984547915,26.6459623860381,-6.69258458190853));
#38436=CARTESIAN_POINT('Ctrl Pts',(-24.441791768956,26.6472343507369,-6.69286701556923));
#38437=CARTESIAN_POINT('Ctrl Pts',(-24.4254727360672,26.6519070297736,-6.69391344129753));
#38438=CARTESIAN_POINT('Ctrl Pts',(-24.4135436439128,26.6552484222353,-6.69467936607175));
#38439=CARTESIAN_POINT('Ctrl Pts',(-24.3967198561104,26.6598563953244,-6.69576103317268));
#38440=CARTESIAN_POINT('Ctrl Pts',(-24.3918408839094,26.6611803940777,-6.69607489502089));
#38441=CARTESIAN_POINT('Ctrl Pts',(-24.1480899071814,26.7267113156639,-6.71176409380519));
#38442=CARTESIAN_POINT('Ctrl Pts',(-23.9026746005692,26.7632027887211,-6.72808190413251));
#38443=CARTESIAN_POINT('Ctrl Pts',(-23.6418869964452,26.7717285467714,-6.74570271557174));
#38444=CARTESIAN_POINT('Ctrl Pts',(-23.6282158027444,26.7720883929734,-6.74662695704583));
#38445=CARTESIAN_POINT('Ctrl Pts',(-23.4682901123197,26.7752793658229,-6.75744302728201));
#38446=CARTESIAN_POINT('Ctrl Pts',(-23.3220038552415,26.768236592781,-6.76738836316686));
#38447=CARTESIAN_POINT('Ctrl Pts',(-23.0852428170791,26.7406069782184,-6.78317298490582));
#38448=CARTESIAN_POINT('Ctrl Pts',(-22.9942764340936,26.7260185553216,-6.78915862237911));
#38449=CARTESIAN_POINT('Ctrl Pts',(-22.8971237741738,26.7061344022,-6.79537939939735));
#38450=CARTESIAN_POINT('Ctrl Pts',(-22.8902014730163,26.7046938699783,-6.79582168698848));
#38451=CARTESIAN_POINT('Ctrl Pts',(-22.8811813799679,26.7027857947686,-6.79639671399809));
#38452=CARTESIAN_POINT('Ctrl Pts',(-22.8790793067976,26.7023389332874,-6.79653062843239));
#38453=CARTESIAN_POINT('Ctrl Pts',(-22.8749451391846,26.7014557634545,-6.79679381644827));
#38454=CARTESIAN_POINT('Ctrl Pts',(-22.8729130170935,26.7010195913567,-6.79692309780114));
#38455=CARTESIAN_POINT('Ctrl Pts',(-22.8690449847572,26.7001854467596,-6.79716901030501));
#38456=CARTESIAN_POINT('Ctrl Pts',(-22.8672090141582,26.6997878378281,-6.79728566115296));
#38457=CARTESIAN_POINT('Ctrl Pts',(-22.8630315150596,26.698879308643,-6.79755092148407));
#38458=CARTESIAN_POINT('Ctrl Pts',(-22.8606902112822,26.6983673822963,-6.79769947198312));
#38459=CARTESIAN_POINT('Ctrl Pts',(-22.8534252176272,26.6967703970234,-6.79816006501327));
#38460=CARTESIAN_POINT('Ctrl Pts',(-22.8485034709469,26.6956763885098,-6.79847159287229));
#38461=CARTESIAN_POINT('Ctrl Pts',(-22.8112758581231,26.6873096870835,-6.80082426945411));
#38462=CARTESIAN_POINT('Ctrl Pts',(-22.7790797355391,26.6795506714261,-6.80283792887449));
#38463=CARTESIAN_POINT('Ctrl Pts',(-22.6005994097372,26.6336162164452,-6.81391228267647));
#38464=CARTESIAN_POINT('Ctrl Pts',(-22.4570056797223,26.5856758862014,-6.82249425602943));
#38465=CARTESIAN_POINT('Ctrl Pts',(-22.2349997944474,26.4937472977537,-6.83597994670178));
#38466=CARTESIAN_POINT('Ctrl Pts',(-22.15417869041,26.4562840724277,-6.84093731780547));
#38467=CARTESIAN_POINT('Ctrl Pts',(-22.075035924178,26.4155367276176,-6.84592209196326));
#38468=CARTESIAN_POINT('',(-26.7730025170003,23.5505602810918,-6.6857734492733));
#38469=CARTESIAN_POINT('Ctrl Pts',(-22.075036226743,26.4155368833958,-7.0956801988874));
#38470=CARTESIAN_POINT('Ctrl Pts',(-22.1173458186021,26.4373203408489,-7.09285197813402));
#38471=CARTESIAN_POINT('Ctrl Pts',(-22.1601486433663,26.4581722041659,-7.08999223830819));
#38472=CARTESIAN_POINT('Ctrl Pts',(-22.2147476759432,26.4832884943005,-7.08633994433301));
#38473=CARTESIAN_POINT('Ctrl Pts',(-22.2261107026674,26.4884359138944,-7.08557960749034));
#38474=CARTESIAN_POINT('Ctrl Pts',(-22.2417045345805,26.495391045298,-7.08453576350786));
#38475=CARTESIAN_POINT('Ctrl Pts',(-22.2459098549835,26.497255909096,-7.08425422069601));
#38476=CARTESIAN_POINT('Ctrl Pts',(-22.2530828130088,26.5004184209584,-7.08377392225219));
#38477=CARTESIAN_POINT('Ctrl Pts',(-22.2560484493447,26.5017206149314,-7.08357532270844));
#38478=CARTESIAN_POINT('Ctrl Pts',(-22.2620424372228,26.5043417696139,-7.08317387774061));
#38479=CARTESIAN_POINT('Ctrl Pts',(-22.2650708626406,26.505660549294,-7.08297102645723));
#38480=CARTESIAN_POINT('Ctrl Pts',(-22.2719802971711,26.5086567523792,-7.08250815920913));
#38481=CARTESIAN_POINT('Ctrl Pts',(-22.2758625844821,26.5103311963064,-7.08224804178803));
#38482=CARTESIAN_POINT('Ctrl Pts',(-22.2839930208616,26.5138189217937,-7.08170320411444));
#38483=CARTESIAN_POINT('Ctrl Pts',(-22.2882417928383,26.5156307186978,-7.08141843382931));
#38484=CARTESIAN_POINT('Ctrl Pts',(-22.2994130414969,26.5203660986127,-7.08066954887109));
#38485=CARTESIAN_POINT('Ctrl Pts',(-22.3063418441918,26.5232746020145,-7.08020492136146));
#38486=CARTESIAN_POINT('Ctrl Pts',(-22.3269976508562,26.5318604405088,-7.07881933870097));
#38487=CARTESIAN_POINT('Ctrl Pts',(-22.3407536603263,26.5374670692928,-7.07789599024569));
#38488=CARTESIAN_POINT('Ctrl Pts',(-22.4918210495548,26.59782408541,-7.06774844861374));
#38489=CARTESIAN_POINT('Ctrl Pts',(-22.6326849268887,26.6431521720975,-7.05820692834398));
#38490=CARTESIAN_POINT('Ctrl Pts',(-23.0794918091771,26.7537124533823,-7.02772847224717));
#38491=CARTESIAN_POINT('Ctrl Pts',(-23.3921120053161,26.7842508786824,-7.00594346111637));
#38492=CARTESIAN_POINT('Ctrl Pts',(-23.7389510308225,26.7676613073852,-6.98365442570308));
#38493=CARTESIAN_POINT('Ctrl Pts',(-23.7736516356324,26.7654382866165,-6.98144781362781));
#38494=CARTESIAN_POINT('Ctrl Pts',(-23.8129022421721,26.7622852068095,-6.97898346116106));
#38495=CARTESIAN_POINT('Ctrl Pts',(-23.8174925478907,26.7619065527234,-6.97869574878871));
#38496=CARTESIAN_POINT('Ctrl Pts',(-23.8244413447299,26.7613183459396,-6.97826096903672));
#38497=CARTESIAN_POINT('Ctrl Pts',(-23.8268004181085,26.7611160347441,-6.97811349646143));
#38498=CARTESIAN_POINT('Ctrl Pts',(-23.8309041055925,26.7607595514616,-6.97785719593905));
#38499=CARTESIAN_POINT('Ctrl Pts',(-23.8326488167634,26.7606065570504,-6.97774830127719));
#38500=CARTESIAN_POINT('Ctrl Pts',(-23.8363026138706,26.760283152516,-6.97752040736914));
#38501=CARTESIAN_POINT('Ctrl Pts',(-23.8382116715723,26.7601124616459,-6.97740142462477));
#38502=CARTESIAN_POINT('Ctrl Pts',(-23.8427808745358,26.7596998152658,-6.97711685715279));
#38503=CARTESIAN_POINT('Ctrl Pts',(-23.8454408814307,26.7594562546907,-6.97695136361522));
#38504=CARTESIAN_POINT('Ctrl Pts',(-23.8544728812748,26.7586179250484,-6.97639000251614));
#38505=CARTESIAN_POINT('Ctrl Pts',(-23.8608434572983,26.7580074782208,-6.97599501717646));
#38506=CARTESIAN_POINT('Ctrl Pts',(-23.8759898556084,26.7565105620833,-6.97505811564336));
#38507=CARTESIAN_POINT('Ctrl Pts',(-23.8847639934306,26.7556070281214,-6.97451713523652));
#38508=CARTESIAN_POINT('Ctrl Pts',(-23.9883944473509,26.7445053264176,-6.96814726139866));
#38509=CARTESIAN_POINT('Ctrl Pts',(-24.0827668335682,26.7301348630574,-6.96254010048603));
#38510=CARTESIAN_POINT('Ctrl Pts',(-24.3929908300243,26.6686935193108,-6.94434540273821));
#38511=CARTESIAN_POINT('Ctrl Pts',(-24.6046358150256,26.6036390121805,-6.93228259038697));
#38512=CARTESIAN_POINT('Ctrl Pts',(-24.9751005463444,26.4466080155529,-6.90952257288052));
#38513=CARTESIAN_POINT('Ctrl Pts',(-25.1359171801091,26.3617858744673,-6.89901059125812));
#38514=CARTESIAN_POINT('Ctrl Pts',(-25.2984602616419,26.2576536687111,-6.8872721525688));
#38515=CARTESIAN_POINT('Ctrl Pts',(-25.3081599031581,26.2513657932325,-6.88656730899386));
#38516=CARTESIAN_POINT('Ctrl Pts',(-25.3215491030216,26.2425834642626,-6.8855882177711));
#38517=CARTESIAN_POINT('Ctrl Pts',(-25.3252677163734,26.2401332888831,-6.88531563252637));
#38518=CARTESIAN_POINT('Ctrl Pts',(-25.3316490224655,26.2359096840775,-6.88484672337184));
#38519=CARTESIAN_POINT('Ctrl Pts',(-25.3343141823218,26.2341399779425,-6.88465053984573));
#38520=CARTESIAN_POINT('Ctrl Pts',(-25.3397394681644,26.2305258548636,-6.88425048038202));
#38521=CARTESIAN_POINT('Ctrl Pts',(-25.3424993872764,26.2286811365328,-6.88404659324187));
#38522=CARTESIAN_POINT('Ctrl Pts',(-25.3488623193335,26.2244139412664,-6.88357567561285));
#38523=CARTESIAN_POINT('Ctrl Pts',(-25.352463290908,26.2219884452374,-6.88330853104305));
#38524=CARTESIAN_POINT('Ctrl Pts',(-25.3600152409071,26.2168794853742,-6.88274692846537));
#38525=CARTESIAN_POINT('Ctrl Pts',(-25.3639651744142,26.2141945023446,-6.88245241312538));
#38526=CARTESIAN_POINT('Ctrl Pts',(-25.3744251400753,26.2070502513257,-6.88167042246911));
#38527=CARTESIAN_POINT('Ctrl Pts',(-25.3809247578297,26.2025758579281,-6.88118237125483));
#38528=CARTESIAN_POINT('Ctrl Pts',(-25.5150022003369,26.1095481574146,-6.87107001317482));
#38529=CARTESIAN_POINT('Ctrl Pts',(-25.6360105228576,26.011925932001,-6.86109065822348));
#38530=CARTESIAN_POINT('Ctrl Pts',(-25.9989603615316,25.6730849136204,-6.82827863802334));
#38531=CARTESIAN_POINT('Ctrl Pts',(-26.2098220653563,25.4020771125344,-6.80434910546385));
#38532=CARTESIAN_POINT('Ctrl Pts',(-26.3755670094173,25.1006470714388,-6.78260606012956));
#38533=CARTESIAN_POINT('Ctrl Pts',(-26.3768891157322,25.098235331595,-6.78243239603754));
#38534=CARTESIAN_POINT('Ctrl Pts',(-26.3841887555581,25.0848790514434,-6.78147232153988));
#38535=CARTESIAN_POINT('Ctrl Pts',(-26.3901059238388,25.0739013755126,-6.7806894689974));
#38536=CARTESIAN_POINT('Ctrl Pts',(-26.3976542763349,25.0597007446438,-6.77968507617528));
#38537=CARTESIAN_POINT('Ctrl Pts',(-26.3993438663491,25.0565092063878,-6.77945988059685));
#38538=CARTESIAN_POINT('Ctrl Pts',(-26.4019182442709,25.0516265253749,-6.77911618704658));
#38539=CARTESIAN_POINT('Ctrl Pts',(-26.4028068930261,25.0499374388918,-6.77899744311836));
#38540=CARTESIAN_POINT('Ctrl Pts',(-26.4044736379315,25.0467625557868,-6.77877453249247));
#38541=CARTESIAN_POINT('Ctrl Pts',(-26.4052520716591,25.0452769469915,-6.77867034449198));
#38542=CARTESIAN_POINT('Ctrl Pts',(-26.4070406500133,25.0418570273374,-6.77843077062982));
#38543=CARTESIAN_POINT('Ctrl Pts',(-26.4080499881461,25.0399223012596,-6.77829543676777));
#38544=CARTESIAN_POINT('Ctrl Pts',(-26.4108532613012,25.0345355783827,-6.77791918406981));
#38545=CARTESIAN_POINT('Ctrl Pts',(-26.4126429196638,25.0310813415682,-6.77767853743976));
#38546=CARTESIAN_POINT('Ctrl Pts',(-26.4225778265608,25.0118205777699,-6.77634012993693));
#38547=CARTESIAN_POINT('Ctrl Pts',(-26.4305986098101,24.9959496843555,-6.77525014625295));
#38548=CARTESIAN_POINT('Ctrl Pts',(-26.558006874156,24.7385743345285,-6.75776792089081));
#38549=CARTESIAN_POINT('Ctrl Pts',(-26.6468022420777,24.4830583426913,-6.7430948502729));
#38550=CARTESIAN_POINT('Ctrl Pts',(-26.7413246266661,24.0377640916672,-6.71756414570334));
#38551=CARTESIAN_POINT('Ctrl Pts',(-26.7641076630816,23.8531243596407,-6.70699749982585));
#38552=CARTESIAN_POINT('Ctrl Pts',(-26.7722890630402,23.628514714336,-6.69357089656174));
#38553=CARTESIAN_POINT('Ctrl Pts',(-26.7730010593588,23.5894451301886,-6.69121578420057));
#38554=CARTESIAN_POINT('Ctrl Pts',(-26.7730025294131,23.5503737872535,-6.68883834809843));
#38555=CARTESIAN_POINT('Ctrl Pts',(-26.7730025170003,23.5505602810918,-6.6857734492733));
#38556=CARTESIAN_POINT('Ctrl Pts',(-26.7730124690381,23.4463425963718,-6.67937532444307));
#38557=CARTESIAN_POINT('Ctrl Pts',(-26.7679627933299,23.3422071110475,-6.67297719961285));
#38558=CARTESIAN_POINT('Ctrl Pts',(-26.757903268745,23.2386529302868,-6.66657907478262));
#38559=CARTESIAN_POINT('Ctrl Pts',(-26.747831610793,23.1349738469139,-6.66017323280859));
#38560=CARTESIAN_POINT('Ctrl Pts',(-26.732738095894,23.0318778447628,-6.65376739083454));
#38561=CARTESIAN_POINT('Ctrl Pts',(-26.7127238958344,22.9298555350112,-6.64736154886052));
#38562=CARTESIAN_POINT('Ctrl Pts',(-26.6926648822893,22.8276047886852,-6.64094136366489));
#38563=CARTESIAN_POINT('Ctrl Pts',(-26.6676632424978,22.7264329132961,-6.63452117846929));
#38564=CARTESIAN_POINT('Ctrl Pts',(-26.6378707209527,22.6268179211993,-6.62810099327366));
#38565=CARTESIAN_POINT('Ctrl Pts',(-26.6080410340008,22.5270786619534,-6.62167279906159));
#38566=CARTESIAN_POINT('Ctrl Pts',(-26.5734086736759,22.4289005179355,-6.6152446048495));
#38567=CARTESIAN_POINT('Ctrl Pts',(-26.5341737343046,22.3327420310774,-6.60881641063743));
#38568=CARTESIAN_POINT('Ctrl Pts',(-26.4948529598919,22.2363731764238,-6.60237415333963));
#38569=CARTESIAN_POINT('Ctrl Pts',(-26.4509096472389,22.1420331531882,-6.59593189604183));
#38570=CARTESIAN_POINT('Ctrl Pts',(-26.4025903952307,22.0501571098174,-6.58948963874403));
#38571=CARTESIAN_POINT('Ctrl Pts',(-26.3861217244632,22.0188429597257,-6.5872939215086));
#38572=CARTESIAN_POINT('Ctrl Pts',(-26.3691450929648,21.9878147911742,-6.58509820427316));
#38573=CARTESIAN_POINT('Ctrl Pts',(-26.3516713914095,21.9570890325732,-6.58290248703773));
#38574=CARTESIAN_POINT('Ctrl Pts',(-26.3025533721021,21.870719902402,-6.5767303957254));
#38575=CARTESIAN_POINT('Ctrl Pts',(-26.2493508985205,21.7864722856375,-6.57055830441309));
#38576=CARTESIAN_POINT('Ctrl Pts',(-26.1922721870792,21.7047580984706,-6.56438621310076));
#38577=CARTESIAN_POINT('Ctrl Pts',(-26.1352708116489,21.6231546259487,-6.55822248436198));
#38578=CARTESIAN_POINT('Ctrl Pts',(-26.0744038836727,21.5440781134574,-6.55205875562318));
#38579=CARTESIAN_POINT('Ctrl Pts',(-26.0099251284088,21.4679153160946,-6.54589502688439));
#38580=CARTESIAN_POINT('Ctrl Pts',(-25.9455146823345,21.3918332060673,-6.53973782803771));
#38581=CARTESIAN_POINT('Ctrl Pts',(-25.8775002953205,21.3186590040293,-6.53358062919102));
#38582=CARTESIAN_POINT('Ctrl Pts',(-25.80617798152,21.2487491258031,-6.52742343034434));
#38583=CARTESIAN_POINT('Ctrl Pts',(-25.7349078000058,21.1788903474585,-6.52127073203664));
#38584=CARTESIAN_POINT('Ctrl Pts',(-25.6603348081736,21.1122914522744,-6.51511803372894));
#38585=CARTESIAN_POINT('Ctrl Pts',(-25.5827935278875,21.0492737910221,-6.50896533542124));
#38586=CARTESIAN_POINT('Ctrl Pts',(-25.5052816513651,20.9862800261566,-6.50281497022548));
#38587=CARTESIAN_POINT('Ctrl Pts',(-25.4248040596408,20.9268650705392,-6.49666460502974));
#38588=CARTESIAN_POINT('Ctrl Pts',(-25.3417294983502,20.8713109794312,-6.49051423983398));
#38589=CARTESIAN_POINT('Ctrl Pts',(-25.2586642141615,20.8157630921595,-6.48436456146178));
#38590=CARTESIAN_POINT('Ctrl Pts',(-25.1730028980841,20.7640754536891,-6.47821488308955));
#38591=CARTESIAN_POINT('Ctrl Pts',(-25.0851436707897,20.7164870591072,-6.47206520471734));
#38592=CARTESIAN_POINT('Ctrl Pts',(-24.997270750165,20.6688912476196,-6.46591456788488));
#38593=CARTESIAN_POINT('Ctrl Pts',(-24.9071996199251,20.6253961559289,-6.45976393105243));
#38594=CARTESIAN_POINT('Ctrl Pts',(-24.8153525073361,20.586194567664,-6.45361329421998));
#38595=CARTESIAN_POINT('Ctrl Pts',(-24.7234071376307,20.5469510419346,-6.44745607749816));
#38596=CARTESIAN_POINT('Ctrl Pts',(-24.62968239192,20.5120103625511,-6.44129886077633));
#38597=CARTESIAN_POINT('Ctrl Pts',(-24.5346198538001,20.4815168738589,-6.43514164405451));
#38598=CARTESIAN_POINT('Ctrl Pts',(-24.4395042806794,20.4510063729741,-6.42898099224669));
#38599=CARTESIAN_POINT('Ctrl Pts',(-24.3430498481901,20.4249481170937,-6.42282034043888));
#38600=CARTESIAN_POINT('Ctrl Pts',(-24.2457106157175,20.4034357884016,-6.41665968863106));
#38601=CARTESIAN_POINT('Ctrl Pts',(-24.148208500095,20.3818874619337,-6.41048872786202));
#38602=CARTESIAN_POINT('Ctrl Pts',(-24.0498190553298,20.3649003313019,-6.40431776709301));
#38603=CARTESIAN_POINT('Ctrl Pts',(-23.9510039263868,20.3525164759585,-6.39814680632398));
#38604=CARTESIAN_POINT('Ctrl Pts',(-23.8755764831212,20.3430636466568,-6.3934363961036));
#38605=CARTESIAN_POINT('Ctrl Pts',(-23.7999011706109,20.336291874113,-6.38872598588321));
#38606=CARTESIAN_POINT('Ctrl Pts',(-23.7241830036435,20.3321994318483,-6.38401557566283));
#38607=CARTESIAN_POINT('Ctrl Pts',(-23.6249688336115,20.3268370693011,-6.3778434843505));
#38608=CARTESIAN_POINT('Ctrl Pts',(-23.5253317077164,20.3260577945984,-6.37167139303816));
#38609=CARTESIAN_POINT('Ctrl Pts',(-23.4257307277596,20.3299090899407,-6.36549930172583));
#38610=CARTESIAN_POINT('Ctrl Pts',(-23.3262646972838,20.3337551671586,-6.35933557298705));
#38611=CARTESIAN_POINT('Ctrl Pts',(-23.2268351456562,20.3422193276125,-6.35317184424825));
#38612=CARTESIAN_POINT('Ctrl Pts',(-23.127904605688,20.3552971655117,-6.34700811550947));
#38613=CARTESIAN_POINT('Ctrl Pts',(-23.0290788733417,20.3683611486691,-6.34085091666278));
#38614=CARTESIAN_POINT('Ctrl Pts',(-22.9307515299165,20.3860290353501,-6.33469371781609));
#38615=CARTESIAN_POINT('Ctrl Pts',(-22.8333824422229,20.4082444417426,-6.3285365189694));
#38616=CARTESIAN_POINT('Ctrl Pts',(-22.7360845254279,20.4304436100201,-6.32238382066169));
#38617=CARTESIAN_POINT('Ctrl Pts',(-22.6397438940379,20.4571835930782,-6.31623112235399));
#38618=CARTESIAN_POINT('Ctrl Pts',(-22.5448117290975,20.4883566557745,-6.31007842404628));
#38619=CARTESIAN_POINT('Ctrl Pts',(-22.4499155625693,20.5195178976012,-6.30392805885053));
#38620=CARTESIAN_POINT('Ctrl Pts',(-22.3564272135155,20.5551087435017,-6.29777769365479));
#38621=CARTESIAN_POINT('Ctrl Pts',(-22.2647833024081,20.5949714244121,-6.29162732845904));
#38622=CARTESIAN_POINT('Ctrl Pts',(-22.1731496253589,20.6348296537774,-6.28547765008684));
#38623=CARTESIAN_POINT('Ctrl Pts',(-22.0833603751052,20.6789585964522,-6.27932797171462));
#38624=CARTESIAN_POINT('Ctrl Pts',(-21.9958318233241,20.7271524938121,-6.27317829334241));
#38625=CARTESIAN_POINT('Ctrl Pts',(-21.9082896297502,20.7753539024485,-6.26702765650995));
#38626=CARTESIAN_POINT('Ctrl Pts',(-21.8230092150584,20.8276213146083,-6.26087701967752));
#38627=CARTESIAN_POINT('Ctrl Pts',(-21.7403810030875,20.8837037111326,-6.25472638284506));
#38628=CARTESIAN_POINT('Ctrl Pts',(-21.6576643962871,20.93984610404,-6.24856916612324));
#38629=CARTESIAN_POINT('Ctrl Pts',(-21.5776060181478,20.999811386696,-6.24241194940142));
#38630=CARTESIAN_POINT('Ctrl Pts',(-21.5005660026429,21.0633060716501,-6.2362547326796));
#38631=CARTESIAN_POINT('Ctrl Pts',(-21.423483006829,21.1268361800289,-6.23009408087179));
#38632=CARTESIAN_POINT('Ctrl Pts',(-21.3494220491909,21.1938993204271,-6.22393342906399));
#38633=CARTESIAN_POINT('Ctrl Pts',(-21.2787073844689,21.2641641242574,-6.21777277725619));
#38634=CARTESIAN_POINT('Ctrl Pts',(-21.2078743889662,21.3345465060909,-6.21160181648715));
#38635=CARTESIAN_POINT('Ctrl Pts',(-21.1403991650312,21.4081409325322,-6.20543085571809));
#38636=CARTESIAN_POINT('Ctrl Pts',(-21.0765666534871,21.4845817596546,-6.19925989494905));
#38637=CARTESIAN_POINT('Ctrl Pts',(-21.0278420989123,21.5429304782428,-6.19454948472867));
#38638=CARTESIAN_POINT('Ctrl Pts',(-20.9812391785367,21.6029369582211,-6.18983907450831));
#38639=CARTESIAN_POINT('Ctrl Pts',(-20.9368672590285,21.664427783974,-6.18512866428793));
#38640=CARTESIAN_POINT('Ctrl Pts',(-20.8787263485569,21.7449997455783,-6.1789565729756));
#38641=CARTESIAN_POINT('Ctrl Pts',(-20.8242126412108,21.8284049003175,-6.17278448166328));
#38642=CARTESIAN_POINT('Ctrl Pts',(-20.7736142485484,21.9142826642855,-6.16661239035095));
#38643=CARTESIAN_POINT('Ctrl Pts',(-20.7230844117058,22.0000440723734,-6.16044866161216));
#38644=CARTESIAN_POINT('Ctrl Pts',(-20.6764595641369,22.0882710599578,-6.15428493287338));
#38645=CARTESIAN_POINT('Ctrl Pts',(-20.6339860177686,22.1785721089075,-6.1481212041346));
#38646=CARTESIAN_POINT('Ctrl Pts',(-20.5915574681364,22.268777492371,-6.14196400528791));
#38647=CARTESIAN_POINT('Ctrl Pts',(-20.553271660124,22.361052177901,-6.13580680644121));
#38648=CARTESIAN_POINT('Ctrl Pts',(-20.5193297345906,22.4549787939932,-6.12964960759453));
#38649=CARTESIAN_POINT('Ctrl Pts',(-20.4854126185464,22.5488367554249,-6.12349690928682));
#38650=CARTESIAN_POINT('Ctrl Pts',(-20.4558332195076,22.6443438394715,-6.1173442109791));
#38651=CARTESIAN_POINT('Ctrl Pts',(-20.430744780573,22.7410622245384,-6.1111915126714));
#38652=CARTESIAN_POINT('Ctrl Pts',(-20.4056658552102,22.8377439338561,-6.10504114747564));
#38653=CARTESIAN_POINT('Ctrl Pts',(-20.3850746151023,22.9356356114981,-6.09889078227992));
#38654=CARTESIAN_POINT('Ctrl Pts',(-20.3690743383633,23.0342846404682,-6.09274041708416));
#38655=CARTESIAN_POINT('Ctrl Pts',(-20.3530758484072,23.1329226531044,-6.08659073871195));
#38656=CARTESIAN_POINT('Ctrl Pts',(-20.3416673720872,23.2323174201236,-6.08044106033971));
#38657=CARTESIAN_POINT('Ctrl Pts',(-20.3349008137088,23.3320075039202,-6.0742913819675));
#38658=CARTESIAN_POINT('Ctrl Pts',(-20.328133200726,23.4317131249495,-6.06814074513503));
#38659=CARTESIAN_POINT('Ctrl Pts',(-20.3260089720974,23.531713720731,-6.06199010830256));
#38660=CARTESIAN_POINT('Ctrl Pts',(-20.3285279818287,23.6315451346419,-6.05583947147009));
#38661=CARTESIAN_POINT('Ctrl Pts',(-20.3310496863713,23.7314833471941,-6.04968225474828));
#38662=CARTESIAN_POINT('Ctrl Pts',(-20.3382245374823,23.8312515813462,-6.04352503802647));
#38663=CARTESIAN_POINT('Ctrl Pts',(-20.3500002869252,23.9303882079353,-6.03736782130466));
#38664=CARTESIAN_POINT('Ctrl Pts',(-20.3617826060106,24.0295801424424,-6.03120716949684));
#38665=CARTESIAN_POINT('Ctrl Pts',(-20.3781708639595,24.1281393391101,-6.02504651768902));
#38666=CARTESIAN_POINT('Ctrl Pts',(-20.3990615482524,24.2256138782157,-6.0188858658812));
#38667=CARTESIAN_POINT('Ctrl Pts',(-20.419987190089,24.3232515268875,-6.01271490511217));
#38668=CARTESIAN_POINT('Ctrl Pts',(-20.4454301968249,24.4198004722806,-6.00654394434313));
#38669=CARTESIAN_POINT('Ctrl Pts',(-20.4752369686842,24.5148233428566,-6.0003729835741));
#38670=CARTESIAN_POINT('Ctrl Pts',(-20.4979890372935,24.5873560841074,-5.99566257335373));
#38671=CARTESIAN_POINT('Ctrl Pts',(-20.5232826416016,24.6589999492179,-5.99095216313338));
#38672=CARTESIAN_POINT('Ctrl Pts',(-20.5510310014623,24.7295691876834,-5.98624175291302));
#38673=CARTESIAN_POINT('Ctrl Pts',(-20.5873810882621,24.8220142171011,-5.9800711604444));
#38674=CARTESIAN_POINT('Ctrl Pts',(-20.628073333324,24.9129398194747,-5.97390056797578));
#38675=CARTESIAN_POINT('Ctrl Pts',(-20.6729602214789,25.0019090076126,-5.96772997550717));
#38676=CARTESIAN_POINT('Ctrl Pts',(-20.7177909247422,25.09076683307,-5.96156710676552));
#38677=CARTESIAN_POINT('Ctrl Pts',(-20.7668056465855,25.1776727252841,-5.95540423802388));
#38678=CARTESIAN_POINT('Ctrl Pts',(-20.8198082354744,25.2622079948243,-5.94924136928223));
#38679=CARTESIAN_POINT('Ctrl Pts',(-20.8727586662569,25.346660075983,-5.94308456521724));
#38680=CARTESIAN_POINT('Ctrl Pts',(-20.929688936328,25.4287458044922,-5.93692776115223));
#38681=CARTESIAN_POINT('Ctrl Pts',(-20.9903566946544,25.5080704154634,-5.93077095708723));
#38682=CARTESIAN_POINT('Ctrl Pts',(-21.0509809855592,25.5873381916938,-5.92461856426812));
#38683=CARTESIAN_POINT('Ctrl Pts',(-21.1153371783464,25.6638484391644,-5.91846617144903));
#38684=CARTESIAN_POINT('Ctrl Pts',(-21.1831398230338,25.7372356105036,-5.91231377862992));
#38685=CARTESIAN_POINT('Ctrl Pts',(-21.2509238758966,25.8106026587128,-5.90616307282773));
#38686=CARTESIAN_POINT('Ctrl Pts',(-21.3221522135677,25.8808480089752,-5.90001236702551));
#38687=CARTESIAN_POINT('Ctrl Pts',(-21.3964998316802,25.9476400409806,-5.89386166122331));
#38688=CARTESIAN_POINT('Ctrl Pts',(-21.4708333489373,26.0144194051317,-5.88771212197111));
#38689=CARTESIAN_POINT('Ctrl Pts',(-21.5482846440256,26.0777464664712,-5.88156258271889));
#38690=CARTESIAN_POINT('Ctrl Pts',(-21.628493597557,26.1373281319742,-5.87541304346668));
#38691=CARTESIAN_POINT('Ctrl Pts',(-21.7087412223504,26.1969385236741,-5.86926053932797));
#38692=CARTESIAN_POINT('Ctrl Pts',(-21.7917488118925,26.2527996536019,-5.86310803518927));
#38693=CARTESIAN_POINT('Ctrl Pts',(-21.8771254373785,26.3046605059723,-5.85695553105056));
#38694=CARTESIAN_POINT('Ctrl Pts',(-21.9417968217631,26.3439442455095,-5.85229511073273));
#38695=CARTESIAN_POINT('Ctrl Pts',(-22.0078268524888,26.3809335524348,-5.8476346904149));
#38696=CARTESIAN_POINT('Ctrl Pts',(-22.0750360153462,26.4155367745563,-5.84297427009707));
#38697=CARTESIAN_POINT('Origin',(-23.5502525316942,23.5502525316942,-77.3107734492734));
#38698=CARTESIAN_POINT('',(-22.0750357159536,26.4155366204114,-4.34479105736985));
#38699=CARTESIAN_POINT('',(-22.075036015346,26.4155367745563,-4.58978870905188));
#38700=CARTESIAN_POINT('',(-22.0750360153461,26.4155367745563,-77.3107734492734));
#38701=CARTESIAN_POINT('Ctrl Pts',(-22.0750357159536,26.4155366204114,-4.34479105736985));
#38702=CARTESIAN_POINT('Ctrl Pts',(-21.9262750432132,26.3389458743798,-4.35595082401482));
#38703=CARTESIAN_POINT('Ctrl Pts',(-21.7835993653722,26.2508318199401,-4.36736202386383));
#38704=CARTESIAN_POINT('Ctrl Pts',(-21.5651824007717,26.091162495296,-4.38558079714581));
#38705=CARTESIAN_POINT('Ctrl Pts',(-21.484985327817,26.0264192458182,-4.39245034300398));
#38706=CARTESIAN_POINT('Ctrl Pts',(-21.3821897363889,25.9349572982021,-4.40136935074242));
#38707=CARTESIAN_POINT('Ctrl Pts',(-21.3567281602756,25.9115581367451,-4.40358831303293));
#38708=CARTESIAN_POINT('Ctrl Pts',(-21.3184678707426,25.8752439182116,-4.40693121407691));
#38709=CARTESIAN_POINT('Ctrl Pts',(-21.3053944240849,25.862623573236,-4.40807504047152));
#38710=CARTESIAN_POINT('Ctrl Pts',(-21.2896333466181,25.8471490905159,-4.40945514163395));
#38711=CARTESIAN_POINT('Ctrl Pts',(-21.286843621777,25.8444000877064,-4.40969946418793));
#38712=CARTESIAN_POINT('Ctrl Pts',(-21.2825033126537,25.840107511556,-4.41007964358257));
#38713=CARTESIAN_POINT('Ctrl Pts',(-21.280949289184,25.8385674450875,-4.41021577623225));
#38714=CARTESIAN_POINT('Ctrl Pts',(-21.2782066756503,25.8358439220824,-4.41045604789312));
#38715=CARTESIAN_POINT('Ctrl Pts',(-21.2770174472398,25.8346611261924,-4.41056023838447));
#38716=CARTESIAN_POINT('Ctrl Pts',(-21.2744801340551,25.8321335939409,-4.41078255000614));
#38717=CARTESIAN_POINT('Ctrl Pts',(-21.2731323214131,25.8307885950075,-4.41090064923559));
#38718=CARTESIAN_POINT('Ctrl Pts',(-21.2692473427699,25.8269048488036,-4.41124108825666));
#38719=CARTESIAN_POINT('Ctrl Pts',(-21.2667132145419,25.8243630462068,-4.41146318487159));
#38720=CARTESIAN_POINT('Ctrl Pts',(-21.2555303040508,25.8131087288927,-4.41244345124847));
#38721=CARTESIAN_POINT('Ctrl Pts',(-21.2469269497937,25.8043509205023,-4.41319805422413));
#38722=CARTESIAN_POINT('Ctrl Pts',(-21.2362602408905,25.7933678748662,-4.41413453696177));
#38723=CARTESIAN_POINT('Ctrl Pts',(-21.2341498583204,25.7911887581915,-4.41431986223902));
#38724=CARTESIAN_POINT('Ctrl Pts',(-21.0574828389286,25.6082516307316,-4.42983811429788));
#38725=CARTESIAN_POINT('Ctrl Pts',(-20.9046305775353,25.4076674774721,-4.44364048320928));
#38726=CARTESIAN_POINT('Ctrl Pts',(-20.6948242768788,25.0530679601789,-4.46669088191714));
#38727=CARTESIAN_POINT('Ctrl Pts',(-20.6234784176463,24.9088958036751,-4.47574346375745));
#38728=CARTESIAN_POINT('Ctrl Pts',(-20.5409574008587,24.7051402815441,-4.48860886784834));
#38729=CARTESIAN_POINT('Ctrl Pts',(-20.5202501028765,24.6496648884683,-4.49211674646901));
#38730=CARTESIAN_POINT('Ctrl Pts',(-20.4942901748366,24.5738012020162,-4.49693603736281));
#38731=CARTESIAN_POINT('Ctrl Pts',(-20.4876911807252,24.5538838120083,-4.49820330736758));
#38732=CARTESIAN_POINT('Ctrl Pts',(-20.4783269438013,24.5246676455887,-4.50006571791261));
#38733=CARTESIAN_POINT('Ctrl Pts',(-20.4754083611208,24.5154182973626,-4.50065583396195));
#38734=CARTESIAN_POINT('Ctrl Pts',(-20.4702426686145,24.4987863250049,-4.50171794011711));
#38735=CARTESIAN_POINT('Ctrl Pts',(-20.4679802308474,24.4914085100104,-4.5021894246017));
#38736=CARTESIAN_POINT('Ctrl Pts',(-20.4645683970457,24.4801382533538,-4.50291020457211));
#38737=CARTESIAN_POINT('Ctrl Pts',(-20.4633998082474,24.4762516125134,-4.50315887037394));
#38738=CARTESIAN_POINT('Ctrl Pts',(-20.4612911866887,24.4691901437063,-4.50361084392879));
#38739=CARTESIAN_POINT('Ctrl Pts',(-20.4603486975989,24.4660160500881,-4.50381407090868));
#38740=CARTESIAN_POINT('Ctrl Pts',(-20.4583327392942,24.4591882071515,-4.50425138260158));
#38741=CARTESIAN_POINT('Ctrl Pts',(-20.4572608522821,24.4555339993288,-4.50448551873203));
#38742=CARTESIAN_POINT('Ctrl Pts',(-20.45438261327,24.4456569084762,-4.5051186223079));
#38743=CARTESIAN_POINT('Ctrl Pts',(-20.4525885551965,24.4394304877248,-4.50551799081654));
#38744=CARTESIAN_POINT('Ctrl Pts',(-20.4446926389493,24.4117131562315,-4.50729702493826));
#38745=CARTESIAN_POINT('Ctrl Pts',(-20.4387956834593,24.3901649653051,-4.5086833526809));
#38746=CARTESIAN_POINT('Ctrl Pts',(-20.4299250072768,24.3563743370221,-4.51086281973684));
#38747=CARTESIAN_POINT('Ctrl Pts',(-20.4267981545735,24.3441725348637,-4.51165094095547));
#38748=CARTESIAN_POINT('Ctrl Pts',(-20.4206339025865,24.3195178272176,-4.51324572502392));
#38749=CARTESIAN_POINT('Ctrl Pts',(-20.4175991068951,24.307064510331,-4.51405245538387));
#38750=CARTESIAN_POINT('Ctrl Pts',(-20.4142687973821,24.293035236027,-4.51496264904633));
#38751=CARTESIAN_POINT('Ctrl Pts',(-20.4139000393392,24.2914766350597,-4.515063787235));
#38752=CARTESIAN_POINT('Ctrl Pts',(-20.4119244060162,24.2830985087457,-4.51560754934112));
#38753=CARTESIAN_POINT('Ctrl Pts',(-20.4103386203709,24.2762740732067,-4.51605083754183));
#38754=CARTESIAN_POINT('Ctrl Pts',(-20.3409299126837,23.9730923382897,-4.5357606624861));
#38755=CARTESIAN_POINT('Ctrl Pts',(-20.3153732059476,23.6686757863615,-4.5564623440001));
#38756=CARTESIAN_POINT('Ctrl Pts',(-20.3410321661644,23.222350528484,-4.5865825014972));
#38757=CARTESIAN_POINT('Ctrl Pts',(-20.3587660258892,23.0801044970532,-4.59610701916792));
#38758=CARTESIAN_POINT('Ctrl Pts',(-20.3889091452484,22.9239325242353,-4.60616713173035));
#38759=CARTESIAN_POINT('Ctrl Pts',(-20.3920276257648,22.9083925571327,-4.60716366477209));
#38760=CARTESIAN_POINT('Ctrl Pts',(-20.3960254110478,22.8892057190212,-4.608387949339));
#38761=CARTESIAN_POINT('Ctrl Pts',(-20.396796531256,22.8855369001591,-4.60862177443541));
#38762=CARTESIAN_POINT('Ctrl Pts',(-20.398020139552,22.8797652948784,-4.60898917145241));
#38763=CARTESIAN_POINT('Ctrl Pts',(-20.3984683307174,22.877661616396,-4.6091229899705));
#38764=CARTESIAN_POINT('Ctrl Pts',(-20.3993093989759,22.8737331891022,-4.60937270778546));
#38765=CARTESIAN_POINT('Ctrl Pts',(-20.3997017526959,22.8719083450851,-4.6094886361724));
#38766=CARTESIAN_POINT('Ctrl Pts',(-20.4005853848317,22.8678158606784,-4.60974846386691));
#38767=CARTESIAN_POINT('Ctrl Pts',(-20.4010775258029,22.8655484143314,-4.6098923124477));
#38768=CARTESIAN_POINT('Ctrl Pts',(-20.4023331689835,22.8597932676649,-4.61025715051243));
#38769=CARTESIAN_POINT('Ctrl Pts',(-20.4031000212082,22.8563062906672,-4.6104779470459));
#38770=CARTESIAN_POINT('Ctrl Pts',(-20.4073379388359,22.8371874381868,-4.61168719781219));
#38771=CARTESIAN_POINT('Ctrl Pts',(-20.4109197558028,22.8215799627082,-4.6126693631131));
#38772=CARTESIAN_POINT('Ctrl Pts',(-20.4861820873531,22.5044900038483,-4.63253379393759));
#38773=CARTESIAN_POINT('Ctrl Pts',(-20.6008718645076,22.2148217555728,-4.64914110241523));
#38774=CARTESIAN_POINT('Ctrl Pts',(-20.8460382011245,21.7876848467198,-4.67697644883709));
#38775=CARTESIAN_POINT('Ctrl Pts',(-20.950146647486,21.63743928333,-4.6875304527898));
#38776=CARTESIAN_POINT('Ctrl Pts',(-21.0721647966423,21.4898446398552,-4.69916290923268));
#38777=CARTESIAN_POINT('Ctrl Pts',(-21.0779618341603,21.4828923290103,-4.69971394672064));
#38778=CARTESIAN_POINT('Ctrl Pts',(-21.0884788797387,21.4703868716219,-4.70071079186515));
#38779=CARTESIAN_POINT('Ctrl Pts',(-21.0931885962287,21.4648251191314,-4.70115617715199));
#38780=CARTESIAN_POINT('Ctrl Pts',(-21.1004914424257,21.4562601938459,-4.70184524054527));
#38781=CARTESIAN_POINT('Ctrl Pts',(-21.1030713417328,21.4532457294312,-4.70208837234911));
#38782=CARTESIAN_POINT('Ctrl Pts',(-21.1078350103882,21.4477004186262,-4.70253676435695));
#38783=CARTESIAN_POINT('Ctrl Pts',(-21.1100171657592,21.4451681877176,-4.70274195751098));
#38784=CARTESIAN_POINT('Ctrl Pts',(-21.1144164638288,21.4400791582594,-4.70315521917378));
#38785=CARTESIAN_POINT('Ctrl Pts',(-21.1166337018437,21.4375224480524,-4.70336329150082));
#38786=CARTESIAN_POINT('Ctrl Pts',(-21.1229672352777,21.4302424123633,-4.70395705293874));
#38787=CARTESIAN_POINT('Ctrl Pts',(-21.1270932661719,21.4255276108418,-4.704343147857));
#38788=CARTESIAN_POINT('Ctrl Pts',(-21.1447688486275,21.4054482343117,-4.70599413223463));
#38789=CARTESIAN_POINT('Ctrl Pts',(-21.1584507481569,21.3902012775273,-4.70726456723108));
#38790=CARTESIAN_POINT('Ctrl Pts',(-21.4104795717445,21.1146736658287,-4.73053503945799));
#38791=CARTESIAN_POINT('Ctrl Pts',(-21.6898020763137,20.8952079582543,-4.75460081916076));
#38792=CARTESIAN_POINT('Ctrl Pts',(-22.1140844665184,20.6622111813712,-4.78713558041646));
#38793=CARTESIAN_POINT('Ctrl Pts',(-22.2329577440848,20.6060880611204,-4.79583583709514));
#38794=CARTESIAN_POINT('Ctrl Pts',(-22.3692751074134,20.5516448146644,-4.80511680044956));
#38795=CARTESIAN_POINT('Ctrl Pts',(-22.383653961665,20.5460215624655,-4.80608731914136));
#38796=CARTESIAN_POINT('Ctrl Pts',(-22.4015440219804,20.5391729685263,-4.80728388699194));
#38797=CARTESIAN_POINT('Ctrl Pts',(-22.4050173503216,20.5378502086811,-4.80751568909807));
#38798=CARTESIAN_POINT('Ctrl Pts',(-22.4104976494858,20.5357739753785,-4.8078806197986));
#38799=CARTESIAN_POINT('Ctrl Pts',(-22.4125030833258,20.5350164960235,-4.80801398952256));
#38800=CARTESIAN_POINT('Ctrl Pts',(-22.4162567761788,20.5336029538071,-4.80826330348295));
#38801=CARTESIAN_POINT('Ctrl Pts',(-22.4180048376903,20.5329464138562,-4.80837927590459));
#38802=CARTESIAN_POINT('Ctrl Pts',(-22.4219355383993,20.5314740113963,-4.80863975890777));
#38803=CARTESIAN_POINT('Ctrl Pts',(-22.4241184877748,20.5306589982547,-4.80878421762349));
#38804=CARTESIAN_POINT('Ctrl Pts',(-22.429678242136,20.5285901086195,-4.80915162805047));
#38805=CARTESIAN_POINT('Ctrl Pts',(-22.433056279022,20.527339520914,-4.80937438206729));
#38806=CARTESIAN_POINT('Ctrl Pts',(-22.4518342381622,20.5204234822103,-4.81061000825419));
#38807=CARTESIAN_POINT('Ctrl Pts',(-22.4672755241837,20.5148699125292,-4.81161626718249));
#38808=CARTESIAN_POINT('Ctrl Pts',(-22.7823357146298,20.404266542287,-4.83196164689188));
#38809=CARTESIAN_POINT('Ctrl Pts',(-23.0958648649883,20.3439251613509,-4.8489239496657));
#38810=CARTESIAN_POINT('Ctrl Pts',(-23.5876807533102,20.3229914005357,-4.87680349048989));
#38811=CARTESIAN_POINT('Ctrl Pts',(-23.762447907284,20.3297595615514,-4.88692890678008));
#38812=CARTESIAN_POINT('Ctrl Pts',(-23.9446881490625,20.3517187417719,-4.89807994762353));
#38813=CARTESIAN_POINT('Ctrl Pts',(-23.9535801870283,20.3528278396286,-4.89862547577618));
#38814=CARTESIAN_POINT('Ctrl Pts',(-23.9696454134781,20.3548997258443,-4.89961372583772));
#38815=CARTESIAN_POINT('Ctrl Pts',(-23.9768202274092,20.3558496230479,-4.90005603863156));
#38816=CARTESIAN_POINT('Ctrl Pts',(-23.9879077508608,20.3573555572028,-4.90074105970012));
#38817=CARTESIAN_POINT('Ctrl Pts',(-23.9918227712544,20.3578946407468,-4.90098323057203));
#38818=CARTESIAN_POINT('Ctrl Pts',(-23.999015638813,20.3588985562542,-4.90142869364828));
#38819=CARTESIAN_POINT('Ctrl Pts',(-24.0022937843447,20.3593612410609,-4.90163191751159));
#38820=CARTESIAN_POINT('Ctrl Pts',(-24.0089231181076,20.3603073409678,-4.90204330908025));
#38821=CARTESIAN_POINT('Ctrl Pts',(-24.0122742685986,20.3607909876138,-4.90225148389443));
#38822=CARTESIAN_POINT('Ctrl Pts',(-24.0218323906047,20.3621858203471,-4.90284585514284));
#38823=CARTESIAN_POINT('Ctrl Pts',(-24.0280374468001,20.3631098468846,-4.90323245872544));
#38824=CARTESIAN_POINT('Ctrl Pts',(-24.05456090029,20.3671387872321,-4.90488819944509));
#38825=CARTESIAN_POINT('Ctrl Pts',(-24.0748516835591,20.3704198727079,-4.90616292163981));
#38826=CARTESIAN_POINT('Ctrl Pts',(-24.4334012536843,20.4319237026631,-4.92883464387146));
#38827=CARTESIAN_POINT('Ctrl Pts',(-24.7601862213466,20.5436161585164,-4.95216928779469));
#38828=CARTESIAN_POINT('Ctrl Pts',(-25.198225977516,20.7764962408265,-4.98557670102779));
#38829=CARTESIAN_POINT('Ctrl Pts',(-25.3280917825407,20.8578853082174,-4.99573715686729));
#38830=CARTESIAN_POINT('Ctrl Pts',(-25.4563262540549,20.9515926029174,-5.00568447582307));
#38831=CARTESIAN_POINT('Ctrl Pts',(-25.4609482330473,20.9549890771403,-5.00604287650497));
#38832=CARTESIAN_POINT('Ctrl Pts',(-25.4676152467896,20.9599158152456,-5.00655963313597));
#38833=CARTESIAN_POINT('Ctrl Pts',(-25.4696675348971,20.9614361744745,-5.00671867442246));
#38834=CARTESIAN_POINT('Ctrl Pts',(-25.4732400807271,20.964089342112,-5.00699547120869));
#38835=CARTESIAN_POINT('Ctrl Pts',(-25.4747611479507,20.9652210535657,-5.0071133039019));
#38836=CARTESIAN_POINT('Ctrl Pts',(-25.4777081617398,20.9674177471659,-5.0073415647418));
#38837=CARTESIAN_POINT('Ctrl Pts',(-25.4791342210247,20.9684825654563,-5.00745200399998));
#38838=CARTESIAN_POINT('Ctrl Pts',(-25.4825428912996,20.9710321719752,-5.00771594730981));
#38839=CARTESIAN_POINT('Ctrl Pts',(-25.4845246776288,20.9725180683774,-5.0078693731546));
#38840=CARTESIAN_POINT('Ctrl Pts',(-25.4916277505714,20.9778565877993,-5.00841917986982));
#38841=CARTESIAN_POINT('Ctrl Pts',(-25.4967393001716,20.9817222331667,-5.00881465031076));
#38842=CARTESIAN_POINT('Ctrl Pts',(-25.5732289574676,21.0399275404345,-5.01473030203032));
#38843=CARTESIAN_POINT('Ctrl Pts',(-25.642327047265,21.0972150550783,-5.02004571108081));
#38844=CARTESIAN_POINT('Ctrl Pts',(-25.9304148951288,21.3571029489143,-5.04252439438099));
#38845=CARTESIAN_POINT('Ctrl Pts',(-26.1230815483506,21.5866699005502,-5.05853233708837));
#38846=CARTESIAN_POINT('Ctrl Pts',(-26.3252470887504,21.909419241752,-5.08051184444434));
#38847=CARTESIAN_POINT('Ctrl Pts',(-26.3663515527543,21.9810127932429,-5.08534804757117));
#38848=CARTESIAN_POINT('Ctrl Pts',(-26.4243610719716,22.0916853103813,-5.09281834347135));
#38849=CARTESIAN_POINT('Ctrl Pts',(-26.4433161068319,22.1296536689628,-5.09537996966839));
#38850=CARTESIAN_POINT('Ctrl Pts',(-26.4647716943873,22.1748423183364,-5.09843116073839));
#38851=CARTESIAN_POINT('Ctrl Pts',(-26.4680038142218,22.1817121937915,-5.09889508562148));
#38852=CARTESIAN_POINT('Ctrl Pts',(-26.4729235547115,22.192265760456,-5.09960789076394));
#38853=CARTESIAN_POINT('Ctrl Pts',(-26.4746285693484,22.1959413526076,-5.09985616838796));
#38854=CARTESIAN_POINT('Ctrl Pts',(-26.4777276056931,22.2026552520006,-5.10030972086817));
#38855=CARTESIAN_POINT('Ctrl Pts',(-26.4791238422937,22.2056925356599,-5.1005149188255));
#38856=CARTESIAN_POINT('Ctrl Pts',(-26.4819235353749,22.2118078624067,-5.10092810403071));
#38857=CARTESIAN_POINT('Ctrl Pts',(-26.4833268759036,22.2148859536462,-5.1011360949586));
#38858=CARTESIAN_POINT('Ctrl Pts',(-26.4873127350398,22.2236651442848,-5.10172937209268));
#38859=CARTESIAN_POINT('Ctrl Pts',(-26.4898834854236,22.2293715417857,-5.10211506304213));
#38860=CARTESIAN_POINT('Ctrl Pts',(-26.5007753394305,22.2537379118671,-5.10376227840026));
#38861=CARTESIAN_POINT('Ctrl Pts',(-26.5089353716632,22.2724689741585,-5.10502931713618));
#38862=CARTESIAN_POINT('Ctrl Pts',(-26.6543177808281,22.6150494472894,-5.12822077501145));
#38863=CARTESIAN_POINT('Ctrl Pts',(-26.7377597233024,22.9590757790159,-5.15219486594882));
#38864=CARTESIAN_POINT('Ctrl Pts',(-26.7700306246897,23.3900790454445,-5.18125307643998));
#38865=CARTESIAN_POINT('Ctrl Pts',(-26.7730316194701,23.470734894779,-5.18663061556587));
#38866=CARTESIAN_POINT('Ctrl Pts',(-26.773000885856,23.5553700292207,-5.19215940808207));
#38867=CARTESIAN_POINT('Ctrl Pts',(-26.772992200676,23.5593172587968,-5.19241699913911));
#38868=CARTESIAN_POINT('Ctrl Pts',(-26.7729306837212,23.5745534210412,-5.19341025665531));
#38869=CARTESIAN_POINT('Ctrl Pts',(-26.7728257872373,23.5858421957659,-5.19414398873007));
#38870=CARTESIAN_POINT('Ctrl Pts',(-26.7726107844339,23.6006216213051,-5.19510153879008));
#38871=CARTESIAN_POINT('Ctrl Pts',(-26.7725543210756,23.6041128372488,-5.19532750878273));
#38872=CARTESIAN_POINT('Ctrl Pts',(-26.7716801497736,23.6532273763693,-5.19850325178169));
#38873=CARTESIAN_POINT('Ctrl Pts',(-26.7698991853338,23.6988313936406,-5.20141308110938));
#38874=CARTESIAN_POINT('Ctrl Pts',(-26.766850391112,23.7493518345502,-5.2045821843114));
#38875=CARTESIAN_POINT('Ctrl Pts',(-26.7665391500096,23.7543179899248,-5.20489312234184));
#38876=CARTESIAN_POINT('Ctrl Pts',(-26.766056743353,23.7617398700845,-5.20535692274102));
#38877=CARTESIAN_POINT('Ctrl Pts',(-26.7658942657873,23.7641961225763,-5.20551026990623));
#38878=CARTESIAN_POINT('Ctrl Pts',(-26.7656097422638,23.7684238494932,-5.20577395776365));
#38879=CARTESIAN_POINT('Ctrl Pts',(-26.7654890465304,23.7701954087584,-5.20588437477081));
#38880=CARTESIAN_POINT('Ctrl Pts',(-26.7652362862405,23.7738607252785,-5.20611266439916));
#38881=CARTESIAN_POINT('Ctrl Pts',(-26.7651040127942,23.7757544623268,-5.2062305244568));
#38882=CARTESIAN_POINT('Ctrl Pts',(-26.7647888091015,23.780210533792,-5.20650764853177));
#38883=CARTESIAN_POINT('Ctrl Pts',(-26.7646044878273,23.7827727753503,-5.2066668336005));
#38884=CARTESIAN_POINT('Ctrl Pts',(-26.7639927858379,23.7911362765147,-5.20718591643801));
#38885=CARTESIAN_POINT('Ctrl Pts',(-26.763552758912,23.7969366427267,-5.20754510292771));
#38886=CARTESIAN_POINT('Ctrl Pts',(-26.7624839937884,23.8105366552394,-5.20838543631905));
#38887=CARTESIAN_POINT('Ctrl Pts',(-26.7618425460042,23.8183353061449,-5.20886588491718));
#38888=CARTESIAN_POINT('Ctrl Pts',(-26.7545638965526,23.9030505377378,-5.21407018181042));
#38889=CARTESIAN_POINT('Ctrl Pts',(-26.7451926698301,23.9797143632219,-5.21864806539345));
#38890=CARTESIAN_POINT('Ctrl Pts',(-26.7200182753869,24.138152583034,-5.227970506302));
#38891=CARTESIAN_POINT('Ctrl Pts',(-26.7037823657742,24.219798938637,-5.23269705143083));
#38892=CARTESIAN_POINT('Ctrl Pts',(-26.6418306540216,24.4785225379532,-5.24767286638111));
#38893=CARTESIAN_POINT('Ctrl Pts',(-26.5842075287858,24.652367482908,-5.25775142085251));
#38894=CARTESIAN_POINT('Ctrl Pts',(-26.5049317543387,24.8372351377853,-5.26921086046796));
#38895=CARTESIAN_POINT('Ctrl Pts',(-26.4975642503108,24.8540190588416,-5.27025803610446));
#38896=CARTESIAN_POINT('Ctrl Pts',(-26.4673510152363,24.9212828381584,-5.27448416730267));
#38897=CARTESIAN_POINT('Ctrl Pts',(-26.44334916078,24.9712307587618,-5.27768968353585));
#38898=CARTESIAN_POINT('Ctrl Pts',(-26.4085814255507,25.0390461023386,-5.28215230478788));
#38899=CARTESIAN_POINT('Ctrl Pts',(-26.3989114385256,25.0574661087759,-5.2833758812833));
#38900=CARTESIAN_POINT('Ctrl Pts',(-26.3581550576753,25.1333079753947,-5.28846361160344));
#38901=CARTESIAN_POINT('Ctrl Pts',(-26.3255071523835,25.1898689500585,-5.29237754452833));
#38902=CARTESIAN_POINT('Ctrl Pts',(-26.2867672102419,25.2525083589832,-5.29686403173555));
#38903=CARTESIAN_POINT('Ctrl Pts',(-26.2823411666535,25.2596030446374,-5.29737442467612));
#38904=CARTESIAN_POINT('Ctrl Pts',(-26.2756094076501,25.2703007165445,-5.29814744679312));
#38905=CARTESIAN_POINT('Ctrl Pts',(-26.2733240247171,25.2739165079744,-5.29840932187725));
#38906=CARTESIAN_POINT('Ctrl Pts',(-26.2693414388832,25.2801898196372,-5.29886470863792));
#38907=CARTESIAN_POINT('Ctrl Pts',(-26.267647517608,25.2828494253302,-5.29905809807799));
#38908=CARTESIAN_POINT('Ctrl Pts',(-26.2641107924049,25.2883844505253,-5.2994612506838));
#38909=CARTESIAN_POINT('Ctrl Pts',(-26.2622673166121,25.2912594336717,-5.29967103872305));
#38910=CARTESIAN_POINT('Ctrl Pts',(-26.2579084261283,25.2980335965865,-5.30016626005236));
#38911=CARTESIAN_POINT('Ctrl Pts',(-26.255389158454,25.3019302770749,-5.30045183715298));
#38912=CARTESIAN_POINT('Ctrl Pts',(-26.2470935474671,25.3147009475393,-5.30139011619081));
#38913=CARTESIAN_POINT('Ctrl Pts',(-26.2412819312013,25.3235518418011,-5.3020441400594));
#38914=CARTESIAN_POINT('Ctrl Pts',(-26.1563762627122,25.4514816963234,-5.31155215632337));
#38915=CARTESIAN_POINT('Ctrl Pts',(-26.0695000848169,25.5651805089211,-5.32070500183791));
#38916=CARTESIAN_POINT('Ctrl Pts',(-25.7591269186931,25.919810698572,-5.35170692088824));
#38917=CARTESIAN_POINT('Ctrl Pts',(-25.5064237377026,26.1323624188969,-5.37464979995359));
#38918=CARTESIAN_POINT('Ctrl Pts',(-25.1926477066409,26.3233699070541,-5.39829770559522));
#38919=CARTESIAN_POINT('Ctrl Pts',(-25.1589301247863,26.3430644895458,-5.40078032831415));
#38920=CARTESIAN_POINT('Ctrl Pts',(-25.1202456072937,26.3647271342287,-5.40355569020661));
#38921=CARTESIAN_POINT('Ctrl Pts',(-25.1156236904286,26.3673003981839,-5.40388611478902));
#38922=CARTESIAN_POINT('Ctrl Pts',(-25.1088570172833,26.3710459650826,-5.40436814095746));
#38923=CARTESIAN_POINT('Ctrl Pts',(-25.1067172606642,26.3722272098077,-5.40452031514336));
#38924=CARTESIAN_POINT('Ctrl Pts',(-25.1029246019762,26.3743153070385,-5.404789590547));
#38925=CARTESIAN_POINT('Ctrl Pts',(-25.1012722470377,26.3752231438615,-5.40490675546279));
#38926=CARTESIAN_POINT('Ctrl Pts',(-25.097817838878,26.3771171202993,-5.40515138402798));
#38927=CARTESIAN_POINT('Ctrl Pts',(-25.0960156430802,26.378102984926,-5.40527882975497));
#38928=CARTESIAN_POINT('Ctrl Pts',(-25.0913606202502,26.3806436668404,-5.40560755945363));
#38929=CARTESIAN_POINT('Ctrl Pts',(-25.0885063735002,26.3821958992278,-5.40580867677183));
#38930=CARTESIAN_POINT('Ctrl Pts',(-25.0763265595334,26.3887958322473,-5.40666502333722));
#38931=CARTESIAN_POINT('Ctrl Pts',(-25.0669783183422,26.393801881204,-5.40731760938806));
#38932=CARTESIAN_POINT('Ctrl Pts',(-24.9160307816441,26.4736791714868,-5.41778267063301));
#38933=CARTESIAN_POINT('Ctrl Pts',(-24.7690454485814,26.5379494228179,-5.42695541724512));
#38934=CARTESIAN_POINT('Ctrl Pts',(-24.3529053209454,26.6840563980972,-5.4517926255825));
#38935=CARTESIAN_POINT('Ctrl Pts',(-24.0769423114776,26.7420497390921,-5.467144767834));
#38936=CARTESIAN_POINT('Ctrl Pts',(-23.7860933963628,26.7643799962144,-5.48439319326439));
#38937=CARTESIAN_POINT('Ctrl Pts',(-23.7752259301992,26.7651589436305,-5.48503899268572));
#38938=CARTESIAN_POINT('Ctrl Pts',(-23.7107189443913,26.7694539315506,-5.48888056175493));
#38939=CARTESIAN_POINT('Ctrl Pts',(-23.6570047554342,26.7716824255818,-5.49211338935558));
#38940=CARTESIAN_POINT('Ctrl Pts',(-23.5944897572586,26.7727108492281,-5.49592349902234));
#38941=CARTESIAN_POINT('Ctrl Pts',(-23.5857167574082,26.772819338863,-5.49645927227084));
#38942=CARTESIAN_POINT('Ctrl Pts',(-23.57264732087,26.7729275842348,-5.49725908209659));
#38943=CARTESIAN_POINT('Ctrl Pts',(-23.568351099801,26.7729545753834,-5.49752226337158));
#38944=CARTESIAN_POINT('Ctrl Pts',(-23.5606913623404,26.7729873806383,-5.49799196775458));
#38945=CARTESIAN_POINT('Ctrl Pts',(-23.5573278603499,26.7729965201878,-5.4981983861593));
#38946=CARTESIAN_POINT('Ctrl Pts',(-23.5502397263787,26.7730046840094,-5.49863373452073));
#38947=CARTESIAN_POINT('Ctrl Pts',(-23.5465151003408,26.7730025168524,-5.49886270158218));
#38948=CARTESIAN_POINT('Ctrl Pts',(-23.5366841725237,26.7729797540248,-5.49946758662873));
#38949=CARTESIAN_POINT('Ctrl Pts',(-23.5305779326432,26.7729482603121,-5.49984384624813));
#38950=CARTESIAN_POINT('Ctrl Pts',(-23.503464402862,26.7727313562464,-5.501517023538));
#38951=CARTESIAN_POINT('Ctrl Pts',(-23.4824595116011,26.7723578956534,-5.50281983113482));
#38952=CARTESIAN_POINT('Ctrl Pts',(-23.3300707220396,26.7681577250595,-5.51232112681596));
#38953=CARTESIAN_POINT('Ctrl Pts',(-23.1990432324052,26.7565023653579,-5.52076560422306));
#38954=CARTESIAN_POINT('Ctrl Pts',(-22.8105136512479,26.697838718788,-5.54663305154377));
#38955=CARTESIAN_POINT('Ctrl Pts',(-22.5576691741607,26.6274701178797,-5.56465311847542));
#38956=CARTESIAN_POINT('Ctrl Pts',(-22.2342596456139,26.4934027281094,-5.58791243245908));
#38957=CARTESIAN_POINT('Ctrl Pts',(-22.1538293697159,26.4561042185385,-5.59370450105131));
#38958=CARTESIAN_POINT('Ctrl Pts',(-22.0750360126322,26.415536773159,-5.59931610453398));
#38959=CARTESIAN_POINT('',(-26.773001157643,23.5472765537013,-5.43577344933047));
#38960=CARTESIAN_POINT('Ctrl Pts',(-22.0750360153462,26.4155367745563,-5.84297427009707));
#38961=CARTESIAN_POINT('Ctrl Pts',(-22.1638664037002,26.4612718726988,-5.8368145899415));
#38962=CARTESIAN_POINT('Ctrl Pts',(-22.2547570412907,26.5028369104112,-5.83065490978592));
#38963=CARTESIAN_POINT('Ctrl Pts',(-22.3472759868601,26.5400627255157,-5.82449522963034));
#38964=CARTESIAN_POINT('Ctrl Pts',(-22.4402513107283,26.5774721684606,-5.8183051649483));
#38965=CARTESIAN_POINT('Ctrl Pts',(-22.5348706286827,26.6104993280361,-5.81211510026625));
#38966=CARTESIAN_POINT('Ctrl Pts',(-22.6306812321648,26.6390235150437,-5.80592503558421));
#38967=CARTESIAN_POINT('Ctrl Pts',(-22.7264918356468,26.6675477020513,-5.79973497090217));
#38968=CARTESIAN_POINT('Ctrl Pts',(-22.8234932841265,26.6915688712652,-5.7935449062201));
#38969=CARTESIAN_POINT('Ctrl Pts',(-22.9212250381291,26.7110185741021,-5.78735484153806));
#38970=CARTESIAN_POINT('Ctrl Pts',(-23.0186730198225,26.7304118031027,-5.78118275022576));
#38971=CARTESIAN_POINT('Ctrl Pts',(-23.1171903225698,26.7453284107951,-5.77501065891346));
#38972=CARTESIAN_POINT('Ctrl Pts',(-23.2163292355858,26.7556562184108,-5.76883856760114));
#38973=CARTESIAN_POINT('Ctrl Pts',(-23.3153338251759,26.7659700328681,-5.76267483886235));
#38974=CARTESIAN_POINT('Ctrl Pts',(-23.4149579227767,26.7717073603206,-5.75651111012354));
#38975=CARTESIAN_POINT('Ctrl Pts',(-23.5147430549401,26.7728068973428,-5.75034738138476));
#38976=CARTESIAN_POINT('Ctrl Pts',(-23.6144224741215,26.7739052695087,-5.74419018253806));
#38977=CARTESIAN_POINT('Ctrl Pts',(-23.7142621567178,26.7703756145777,-5.73803298369135));
#38978=CARTESIAN_POINT('Ctrl Pts',(-23.813798889093,26.762208459163,-5.73187578484465));
#38979=CARTESIAN_POINT('Ctrl Pts',(-23.9132628661526,26.7540472734436,-5.72572308653695));
#38980=CARTESIAN_POINT('Ctrl Pts',(-24.0124239016077,26.7412553620142,-5.71957038822927));
#38981=CARTESIAN_POINT('Ctrl Pts',(-24.1108200893969,26.723875315793,-5.71341768992157));
#38982=CARTESIAN_POINT('Ctrl Pts',(-24.2091789652119,26.7065018601101,-5.70726732472582));
#38983=CARTESIAN_POINT('Ctrl Pts',(-24.306773142346,26.6845438021302,-5.70111695953007));
#38984=CARTESIAN_POINT('Ctrl Pts',(-24.4031480246445,26.6580953270436,-5.69496659433432));
#38985=CARTESIAN_POINT('Ctrl Pts',(-24.4995121445675,26.6316498055109,-5.68881691596212));
#38986=CARTESIAN_POINT('Ctrl Pts',(-24.5946568214479,26.6007149787936,-5.6826672375899));
#38987=CARTESIAN_POINT('Ctrl Pts',(-24.6881407888652,26.5654354244376,-5.6765175592177));
#38988=CARTESIAN_POINT('Ctrl Pts',(-24.7816393262585,26.5301503715744,-5.67036692238525));
#38989=CARTESIAN_POINT('Ctrl Pts',(-24.8734762336229,26.4905193994746,-5.66421628555281));
#38990=CARTESIAN_POINT('Ctrl Pts',(-24.963229405051,26.4467355573408,-5.65806564872037));
#38991=CARTESIAN_POINT('Ctrl Pts',(-25.0530785935183,26.4029048756934,-5.65190843199856));
#38992=CARTESIAN_POINT('Ctrl Pts',(-25.1408392034506,26.3549126432117,-5.64575121527673));
#38993=CARTESIAN_POINT('Ctrl Pts',(-25.2261130828956,26.3029982474164,-5.63959399855491));
#38994=CARTESIAN_POINT('Ctrl Pts',(-25.3114345362888,26.2510548887922,-5.6334333467471));
#38995=CARTESIAN_POINT('Ctrl Pts',(-25.3942661361837,26.1951852520902,-5.6272726949393));
#38996=CARTESIAN_POINT('Ctrl Pts',(-25.474239868565,26.1356713159651,-5.62111204313149));
#38997=CARTESIAN_POINT('Ctrl Pts',(-25.5543474254393,26.0760577918616,-5.61494108236246));
#38998=CARTESIAN_POINT('Ctrl Pts',(-25.6315872262005,26.0127880627121,-5.60877012159343));
#38999=CARTESIAN_POINT('Ctrl Pts',(-25.7056253065707,25.9461836166424,-5.6025991608244));
#39000=CARTESIAN_POINT('Ctrl Pts',(-25.762139963449,25.8953431923989,-5.59788875060405));
#39001=CARTESIAN_POINT('Ctrl Pts',(-25.8167898235724,25.8425605947428,-5.59317834038368));
#39002=CARTESIAN_POINT('Ctrl Pts',(-25.8694420086437,25.787991956316,-5.58846793016333));
#39003=CARTESIAN_POINT('Ctrl Pts',(-25.9405584090568,25.7142870353311,-5.58210566012863));
#39004=CARTESIAN_POINT('Ctrl Pts',(-26.008305078855,25.6370355103818,-5.57574339009394));
#39005=CARTESIAN_POINT('Ctrl Pts',(-26.072303925268,25.5565860858852,-5.56938112005923));
#39006=CARTESIAN_POINT('Ctrl Pts',(-26.1334909052143,25.4796713038342,-5.56329838402811));
#39007=CARTESIAN_POINT('Ctrl Pts',(-26.1912520703198,25.3998340623105,-5.55721564799696));
#39008=CARTESIAN_POINT('Ctrl Pts',(-26.2452931100523,25.3174180144669,-5.55113291196584));
#39009=CARTESIAN_POINT('Ctrl Pts',(-26.2992838720878,25.2350786433324,-5.54505583507748));
#39010=CARTESIAN_POINT('Ctrl Pts',(-26.3495611375826,25.1501656008213,-5.53897875818915));
#39011=CARTESIAN_POINT('Ctrl Pts',(-26.395871428336,25.0630547849894,-5.5329016813008));
#39012=CARTESIAN_POINT('Ctrl Pts',(-26.4421517837701,24.9760002782423,-5.52682853268054));
#39013=CARTESIAN_POINT('Ctrl Pts',(-26.4844700490081,24.886751213229,-5.52075538406026));
#39014=CARTESIAN_POINT('Ctrl Pts',(-26.5226172132757,24.7957105848565,-5.51468223543999));
#39015=CARTESIAN_POINT('Ctrl Pts',(-26.5607505474694,24.7047029628331,-5.50861128861103));
#39016=CARTESIAN_POINT('Ctrl Pts',(-26.5947156143592,24.6119054800709,-5.50254034178209));
#39017=CARTESIAN_POINT('Ctrl Pts',(-26.6243508388008,24.5177426663954,-5.49646939495312));
#39018=CARTESIAN_POINT('Ctrl Pts',(-26.6539931010491,24.4235574908282,-5.49039700638883));
#39019=CARTESIAN_POINT('Ctrl Pts',(-26.6793033267433,24.3280067610761,-5.48432461782454));
#39020=CARTESIAN_POINT('Ctrl Pts',(-26.7001695323316,24.2315310735517,-5.47825222926025));
#39021=CARTESIAN_POINT('Ctrl Pts',(-26.7210387565873,24.1350414291047,-5.47217896221705));
#39022=CARTESIAN_POINT('Ctrl Pts',(-26.7374625987345,24.0376269996952,-5.46610569517386));
#39023=CARTESIAN_POINT('Ctrl Pts',(-26.7493803441058,23.9397378361081,-5.46003242813066));
#39024=CARTESIAN_POINT('Ctrl Pts',(-26.761308029878,23.8417670247347,-5.45395409547252));
#39025=CARTESIAN_POINT('Ctrl Pts',(-26.7687220787112,23.7433211337576,-5.4478757628144));
#39026=CARTESIAN_POINT('Ctrl Pts',(-26.7716137554282,23.6448539519952,-5.44179743015627));
#39027=CARTESIAN_POINT('Ctrl Pts',(-26.7725690286409,23.6123250525822,-5.43978943654768));
#39028=CARTESIAN_POINT('Ctrl Pts',(-26.7730311850157,23.5797938217113,-5.43778144293905));
#39029=CARTESIAN_POINT('Ctrl Pts',(-26.773001157643,23.5472765537013,-5.43577344933045));
#39030=CARTESIAN_POINT('Ctrl Pts',(-26.7730011581167,23.547277066739,-5.43576586302522));
#39031=CARTESIAN_POINT('Ctrl Pts',(-26.7728017003367,23.3312428347102,-5.42115614110461));
#39032=CARTESIAN_POINT('Ctrl Pts',(-26.7508804635188,23.1157498323663,-5.40642471359264));
#39033=CARTESIAN_POINT('Ctrl Pts',(-26.7042487805336,22.8879107697878,-5.39160782088756));
#39034=CARTESIAN_POINT('Ctrl Pts',(-26.7008218005194,22.8717967439381,-5.3905642810244));
#39035=CARTESIAN_POINT('Ctrl Pts',(-26.6957783552933,22.8489445777544,-5.38909131329109));
#39036=CARTESIAN_POINT('Ctrl Pts',(-26.6942635608367,22.8421845943516,-5.3886564537183));
#39037=CARTESIAN_POINT('Ctrl Pts',(-26.6919137736767,22.8318545609168,-5.38799331642536));
#39038=CARTESIAN_POINT('Ctrl Pts',(-26.6910944784316,22.8282810158282,-5.38776416502595));
#39039=CARTESIAN_POINT('Ctrl Pts',(-26.6897395642714,22.8224172022104,-5.3873885752252));
#39040=CARTESIAN_POINT('Ctrl Pts',(-26.6892075358411,22.8201261203171,-5.38724193279483));
#39041=CARTESIAN_POINT('Ctrl Pts',(-26.6881679470201,22.8156714623836,-5.38695701853772));
#39042=CARTESIAN_POINT('Ctrl Pts',(-26.6876606561421,22.8135078256737,-5.38681873127108));
#39043=CARTESIAN_POINT('Ctrl Pts',(-26.6867661552835,22.8097103851889,-5.38657619164215));
#39044=CARTESIAN_POINT('Ctrl Pts',(-26.6863799080287,22.8080763658457,-5.38647188383003));
#39045=CARTESIAN_POINT('Ctrl Pts',(-26.6854934141952,22.8043391017161,-5.38623344272216));
#39046=CARTESIAN_POINT('Ctrl Pts',(-26.6849923290821,22.8022360619118,-5.38609935892889));
#39047=CARTESIAN_POINT('Ctrl Pts',(-26.683627916442,22.7965351105121,-5.38573612872367));
#39048=CARTESIAN_POINT('Ctrl Pts',(-26.6827605050167,22.7929381649124,-5.38550721900772));
#39049=CARTESIAN_POINT('Ctrl Pts',(-26.678649819353,22.7760200440742,-5.38443176691326));
#39050=CARTESIAN_POINT('Ctrl Pts',(-26.6753276915483,22.7627179004519,-5.38358972973967));
#39051=CARTESIAN_POINT('Ctrl Pts',(-26.6159122931846,22.5311100329855,-5.36898436109109));
#39052=CARTESIAN_POINT('Ctrl Pts',(-26.5371437407903,22.3192217469999,-5.35646055239281));
#39053=CARTESIAN_POINT('Ctrl Pts',(-26.4167171715861,22.0766325775321,-5.34132759708626));
#39054=CARTESIAN_POINT('Ctrl Pts',(-26.3956914038968,22.0364319065887,-5.33879298767271));
#39055=CARTESIAN_POINT('Ctrl Pts',(-26.3522304509475,21.9574424810711,-5.33373865440602));
#39056=CARTESIAN_POINT('Ctrl Pts',(-26.3298211103849,21.9186513174497,-5.33121970989232));
#39057=CARTESIAN_POINT('Ctrl Pts',(-26.24028727996,21.7708667053919,-5.32144573235574));
#39058=CARTESIAN_POINT('Ctrl Pts',(-26.1675070609782,21.6654515586953,-5.3140879175494));
#39059=CARTESIAN_POINT('Ctrl Pts',(-26.0543920849133,21.5208448396623,-5.30319900321725));
#39060=CARTESIAN_POINT('Ctrl Pts',(-26.0190007297739,21.4779368606392,-5.29985949201865));
#39061=CARTESIAN_POINT('Ctrl Pts',(-25.9778900924732,21.4306433201386,-5.29604493205236));
#39062=CARTESIAN_POINT('Ctrl Pts',(-25.9732441860066,21.4253339972309,-5.29561474859756));
#39063=CARTESIAN_POINT('Ctrl Pts',(-25.9656552853289,21.4167186813138,-5.29491349866213));
#39064=CARTESIAN_POINT('Ctrl Pts',(-25.9627228310524,21.4134034009899,-5.29464287253148));
#39065=CARTESIAN_POINT('Ctrl Pts',(-25.9570308823807,21.4069950307853,-5.29411824554769));
#39066=CARTESIAN_POINT('Ctrl Pts',(-25.9542722304672,21.4039012016013,-5.29386428033336));
#39067=CARTESIAN_POINT('Ctrl Pts',(-25.9494871613744,21.3985555429547,-5.29342427407203));
#39068=CARTESIAN_POINT('Ctrl Pts',(-25.9474635190695,21.3963012273436,-5.29323835022815));
#39069=CARTESIAN_POINT('Ctrl Pts',(-25.9432605972093,21.3916324772015,-5.29285252886805));
#39070=CARTESIAN_POINT('Ctrl Pts',(-25.9410808358468,21.3892184826289,-5.2926526110712));
#39071=CARTESIAN_POINT('Ctrl Pts',(-25.935132155612,21.3826505844619,-5.29210751386498));
#39072=CARTESIAN_POINT('Ctrl Pts',(-25.9313560538938,21.3785032279863,-5.2917620297103));
#39073=CARTESIAN_POINT('Ctrl Pts',(-25.9170560785965,21.3628794511765,-5.29045567777744));
#39074=CARTESIAN_POINT('Ctrl Pts',(-25.9064600370686,21.3514696408815,-5.28949173224048));
#39075=CARTESIAN_POINT('Ctrl Pts',(-25.7280179470477,21.1620943821326,-5.27332377836745));
#39076=CARTESIAN_POINT('Ctrl Pts',(-25.5405649662978,21.0037706143978,-5.25720247528504));
#39077=CARTESIAN_POINT('Ctrl Pts',(-25.2711385023251,20.8242769072443,-5.23534843579562));
#39078=CARTESIAN_POINT('Ctrl Pts',(-25.2036221445284,20.7828059752931,-5.22997701626038));
#39079=CARTESIAN_POINT('Ctrl Pts',(-25.0619657674111,20.7028314202572,-5.21898369269443));
#39080=CARTESIAN_POINT('Ctrl Pts',(-24.9877145582437,20.6646350937566,-5.21336774464087));
#39081=CARTESIAN_POINT('Ctrl Pts',(-24.8505649054669,20.6006916894435,-5.20334435881736));
#39082=CARTESIAN_POINT('Ctrl Pts',(-24.7881735276325,20.5739671925596,-5.19891002702729));
#39083=CARTESIAN_POINT('Ctrl Pts',(-24.7071649191778,20.5422569667112,-5.19335146602427));
#39084=CARTESIAN_POINT('Ctrl Pts',(-24.6892870854578,20.5354417719173,-5.19213694424257));
#39085=CARTESIAN_POINT('Ctrl Pts',(-24.6604289659922,20.5247341439105,-5.19019725187474));
#39086=CARTESIAN_POINT('Ctrl Pts',(-24.6494867141667,20.520741440434,-5.18946653965968));
#39087=CARTESIAN_POINT('Ctrl Pts',(-24.6361704269276,20.515964125247,-5.18858328187162));
#39088=CARTESIAN_POINT('Ctrl Pts',(-24.6338170052042,20.515122906697,-5.18842740805631));
#39089=CARTESIAN_POINT('Ctrl Pts',(-24.6292695410634,20.5135034022,-5.18812665738464));
#39090=CARTESIAN_POINT('Ctrl Pts',(-24.6270756303461,20.5127247546551,-5.18798175904151));
#39091=CARTESIAN_POINT('Ctrl Pts',(-24.623120514524,20.5113258559694,-5.18772089975285));
#39092=CARTESIAN_POINT('Ctrl Pts',(-24.6213596181994,20.5107047596875,-5.18760488828299));
#39093=CARTESIAN_POINT('Ctrl Pts',(-24.6175742511704,20.5093732982051,-5.18735577647971));
#39094=CARTESIAN_POINT('Ctrl Pts',(-24.6155496162233,20.5086634260968,-5.18722270612757));
#39095=CARTESIAN_POINT('Ctrl Pts',(-24.610097892291,20.5067580683867,-5.18686483964569));
#39096=CARTESIAN_POINT('Ctrl Pts',(-24.6066694771679,20.5055663452071,-5.18664026857999));
#39097=CARTESIAN_POINT('Ctrl Pts',(-24.5909222334664,20.500122375653,-5.18561094811414));
#39098=CARTESIAN_POINT('Ctrl Pts',(-24.5785794693659,20.4959390049154,-5.1848102504434));
#39099=CARTESIAN_POINT('Ctrl Pts',(-24.3633691379464,20.4244495734823,-5.17094934600652));
#39100=CARTESIAN_POINT('Ctrl Pts',(-24.1542904686654,20.377403406481,-5.15900948745388));
#39101=CARTESIAN_POINT('Ctrl Pts',(-23.7777529224431,20.3312830887449,-5.13780880633432));
#39102=CARTESIAN_POINT('Ctrl Pts',(-23.6121413032126,20.323847999034,-5.12858393289394));
#39103=CARTESIAN_POINT('Ctrl Pts',(-23.3382913393247,20.3326517545762,-5.11277056133077));
#39104=CARTESIAN_POINT('Ctrl Pts',(-23.2301373464575,20.3416072119602,-5.10638363243123));
#39105=CARTESIAN_POINT('Ctrl Pts',(-23.1033555528975,20.3585790630121,-5.09864248888314));
#39106=CARTESIAN_POINT('Ctrl Pts',(-23.0840869987578,20.3613363975877,-5.09745909881912));
#39107=CARTESIAN_POINT('Ctrl Pts',(-23.0605136184476,20.3649279712969,-5.09600254877397));
#39108=CARTESIAN_POINT('Ctrl Pts',(-23.0561836761207,20.3655967066683,-5.0957346473616));
#39109=CARTESIAN_POINT('Ctrl Pts',(-23.0477918528838,20.3669103032346,-5.09521471985265));
#39110=CARTESIAN_POINT('Ctrl Pts',(-23.0437298143259,20.3675541146612,-5.09496272752393));
#39111=CARTESIAN_POINT('Ctrl Pts',(-23.0366818087502,20.3686850204978,-5.09452493343813));
#39112=CARTESIAN_POINT('Ctrl Pts',(-23.0336952678335,20.3691685483925,-5.09433924532489));
#39113=CARTESIAN_POINT('Ctrl Pts',(-23.0274849046246,20.3701829969954,-5.09395274801992));
#39114=CARTESIAN_POINT('Ctrl Pts',(-23.0242612012359,20.3707146159615,-5.09375191679583));
#39115=CARTESIAN_POINT('Ctrl Pts',(-23.0163991096025,20.3720234328168,-5.09326161550997));
#39116=CARTESIAN_POINT('Ctrl Pts',(-23.0117616132844,20.3728058819997,-5.09297197847111));
#39117=CARTESIAN_POINT('Ctrl Pts',(-22.9941670918377,20.3758140955516,-5.09187145911698));
#39118=CARTESIAN_POINT('Ctrl Pts',(-22.9812221544401,20.3781089626214,-5.09105837737816));
#39119=CARTESIAN_POINT('Ctrl Pts',(-22.7578611386389,20.419117415314,-5.07696924404707));
#39120=CARTESIAN_POINT('Ctrl Pts',(-22.5518439070098,20.478601725119,-5.06300310952108));
#39121=CARTESIAN_POINT('Ctrl Pts',(-22.2488643231098,20.599803142625,-5.0410936459051));
#39122=CARTESIAN_POINT('Ctrl Pts',(-22.1467163058612,20.6470047092895,-5.03346083206489));
#39123=CARTESIAN_POINT('Ctrl Pts',(-21.9524996474792,20.7493998625349,-5.01862247536965));
#39124=CARTESIAN_POINT('Ctrl Pts',(-21.8602951858603,20.8040484304449,-5.01142331252134));
#39125=CARTESIAN_POINT('Ctrl Pts',(-21.731845526678,20.8891030831865,-5.00132085702342));
#39126=CARTESIAN_POINT('Ctrl Pts',(-21.6932808483685,20.9158689052912,-4.99827806649798));
#39127=CARTESIAN_POINT('Ctrl Pts',(-21.6409243019268,20.9539282665429,-4.99414816115956));
#39128=CARTESIAN_POINT('Ctrl Pts',(-21.6266225226523,20.9645066818396,-4.99302015277972));
#39129=CARTESIAN_POINT('Ctrl Pts',(-21.6036061860228,20.9818275409794,-4.99120598757277));
#39130=CARTESIAN_POINT('Ctrl Pts',(-21.5948375454561,20.9884970460886,-4.99051511732783));
#39131=CARTESIAN_POINT('Ctrl Pts',(-21.5841546482203,20.9967093628273,-4.98967394797627));
#39132=CARTESIAN_POINT('Ctrl Pts',(-21.5822078753946,20.9982094612163,-4.98952068080459));
#39133=CARTESIAN_POINT('Ctrl Pts',(-21.5784440597433,21.0011165616672,-4.98922440447182));
#39134=CARTESIAN_POINT('Ctrl Pts',(-21.5766268030156,21.0025232825548,-4.98908137557956));
#39135=CARTESIAN_POINT('Ctrl Pts',(-21.573337323056,21.0050752688324,-4.98882251289654));
#39136=CARTESIAN_POINT('Ctrl Pts',(-21.5718645939768,21.006219864946,-4.98870663212928));
#39137=CARTESIAN_POINT('Ctrl Pts',(-21.568905599152,21.0085237011212,-4.98847383448321));
#39138=CARTESIAN_POINT('Ctrl Pts',(-21.567419362718,21.0096829618314,-4.98835691997815));
#39139=CARTESIAN_POINT('Ctrl Pts',(-21.5631814255541,21.0129945263142,-4.98802358213339));
#39140=CARTESIAN_POINT('Ctrl Pts',(-21.560432195431,21.0151500098245,-4.98780738614676));
#39141=CARTESIAN_POINT('Ctrl Pts',(-21.5486850904564,21.0243909942745,-4.98688378193596));
#39142=CARTESIAN_POINT('Ctrl Pts',(-21.5397213710201,21.0315200748215,-4.98617945447827));
#39143=CARTESIAN_POINT('Ctrl Pts',(-21.3891023450939,21.1526277343998,-4.97434824413224));
#39144=CARTESIAN_POINT('Ctrl Pts',(-21.257280791091,21.2783642699907,-4.96404086225563));
#39145=CARTESIAN_POINT('Ctrl Pts',(-21.0308774231787,21.5342186070111,-4.94488652539501));
#39146=CARTESIAN_POINT('Ctrl Pts',(-20.9340468847667,21.6615729830931,-4.93603832258459));
#39147=CARTESIAN_POINT('Ctrl Pts',(-20.7851740077278,21.8909219170241,-4.92046990296279));
#39148=CARTESIAN_POINT('Ctrl Pts',(-20.7283800413686,21.9894613179422,-4.91388661078038));
#39149=CARTESIAN_POINT('Ctrl Pts',(-20.6541990567995,22.1355061078755,-4.90413136933178));
#39150=CARTESIAN_POINT('Ctrl Pts',(-20.6325333751819,22.1807461722552,-4.90111038486596));
#39151=CARTESIAN_POINT('Ctrl Pts',(-20.6086924112458,22.233664569667,-4.89757125327117));
#39152=CARTESIAN_POINT('Ctrl Pts',(-20.6054782281746,22.2408694313171,-4.89708928850533));
#39153=CARTESIAN_POINT('Ctrl Pts',(-20.6006098044179,22.2518910076405,-4.89635181226217));
#39154=CARTESIAN_POINT('Ctrl Pts',(-20.5989364283181,22.2556992792507,-4.89609695764449));
#39155=CARTESIAN_POINT('Ctrl Pts',(-20.5960563972188,22.262288265906,-4.89565594867708));
#39156=CARTESIAN_POINT('Ctrl Pts',(-20.594846280828,22.2650674698699,-4.89546991313726));
#39157=CARTESIAN_POINT('Ctrl Pts',(-20.5923483757165,22.2708264478474,-4.89508437297264));
#39158=CARTESIAN_POINT('Ctrl Pts',(-20.5910611649026,22.2738064675952,-4.894884848832));
#39159=CARTESIAN_POINT('Ctrl Pts',(-20.5879502827344,22.2810384625064,-4.89440057752821));
#39160=CARTESIAN_POINT('Ctrl Pts',(-20.586131264607,22.285292421149,-4.8941156718022));
#39161=CARTESIAN_POINT('Ctrl Pts',(-20.5793751237427,22.3011869340001,-4.89305094855348));
#39162=CARTESIAN_POINT('Ctrl Pts',(-20.574497411347,22.3128524764073,-4.89226911022169));
#39163=CARTESIAN_POINT('Ctrl Pts',(-20.4970181477516,22.5012596949878,-4.87963452661291));
#39164=CARTESIAN_POINT('Ctrl Pts',(-20.4402205282917,22.6840519723448,-4.86723778386786));
#39165=CARTESIAN_POINT('Ctrl Pts',(-20.3625729258513,23.0440509627052,-4.84264097773425));
#39166=CARTESIAN_POINT('Ctrl Pts',(-20.3395594746795,23.2201200858849,-4.83053831832784));
#39167=CARTESIAN_POINT('Ctrl Pts',(-20.3268531186829,23.4873279871111,-4.81258149196924));
#39168=CARTESIAN_POINT('Ctrl Pts',(-20.3263548312428,23.5776272335715,-4.80658807722797));
#39169=CARTESIAN_POINT('Ctrl Pts',(-20.3304785236612,23.6905763818779,-4.79927228883979));
#39170=CARTESIAN_POINT('Ctrl Pts',(-20.3315496995399,23.7133095333237,-4.79780910730074));
#39171=CARTESIAN_POINT('Ctrl Pts',(-20.3343997583616,23.7626683108481,-4.79465502020018));
#39172=CARTESIAN_POINT('Ctrl Pts',(-20.3362687215171,23.7892874759925,-4.79296846193282));
#39173=CARTESIAN_POINT('Ctrl Pts',(-20.3388276713078,23.8202283714001,-4.79102728418031));
#39174=CARTESIAN_POINT('Ctrl Pts',(-20.3391960126509,23.8245746415895,-4.79075504824071));
#39175=CARTESIAN_POINT('Ctrl Pts',(-20.3397722862302,23.8312141983763,-4.7903398569693));
#39176=CARTESIAN_POINT('Ctrl Pts',(-20.3399738524266,23.8335080103328,-4.79019654367755));
#39177=CARTESIAN_POINT('Ctrl Pts',(-20.3403272895627,23.8374812663057,-4.78994852164491));
#39178=CARTESIAN_POINT('Ctrl Pts',(-20.3404780199327,23.8391608039072,-4.78984374828197));
#39179=CARTESIAN_POINT('Ctrl Pts',(-20.3407955213803,23.8426676962074,-4.78962512317792));
#39180=CARTESIAN_POINT('Ctrl Pts',(-20.3409625344194,23.8444950216962,-4.78951128563158));
#39181=CARTESIAN_POINT('Ctrl Pts',(-20.3414292903606,23.8495542243269,-4.78919633184865));
#39182=CARTESIAN_POINT('Ctrl Pts',(-20.3417323562048,23.8527858043011,-4.78899540416604));
#39183=CARTESIAN_POINT('Ctrl Pts',(-20.3429435580294,23.8654942570319,-4.78820620342639));
#39184=CARTESIAN_POINT('Ctrl Pts',(-20.3438888150326,23.8749676680965,-4.78762000878183));
#39185=CARTESIAN_POINT('Ctrl Pts',(-20.3603017654807,24.0323948000153,-4.77791175520961));
#39186=CARTESIAN_POINT('Ctrl Pts',(-20.3859558691113,24.1791297114637,-4.7693445829478));
#39187=CARTESIAN_POINT('Ctrl Pts',(-20.4699443666183,24.5189131341003,-4.74956994853492));
#39188=CARTESIAN_POINT('Ctrl Pts',(-20.5364111285628,24.7092879196807,-4.73851792459834));
#39189=CARTESIAN_POINT('Ctrl Pts',(-20.6497377678543,24.95672499005,-4.72299344350883));
#39190=CARTESIAN_POINT('Ctrl Pts',(-20.681399754507,25.0202299236836,-4.71890164379641));
#39191=CARTESIAN_POINT('Ctrl Pts',(-20.7551536077435,25.1566848238478,-4.7098136680943));
#39192=CARTESIAN_POINT('Ctrl Pts',(-20.7980596886749,25.2291317219921,-4.70479441932454));
#39193=CARTESIAN_POINT('Ctrl Pts',(-20.8489765755297,25.3078982541905,-4.69908291239882));
#39194=CARTESIAN_POINT('Ctrl Pts',(-20.8542400305717,25.3159611338673,-4.69849521174591));
#39195=CARTESIAN_POINT('Ctrl Pts',(-20.8620251109924,25.3277708277269,-4.69762987249399));
#39196=CARTESIAN_POINT('Ctrl Pts',(-20.8645186394031,25.3315361749172,-4.69735329077408));
#39197=CARTESIAN_POINT('Ctrl Pts',(-20.8689003316166,25.3381226235672,-4.6968682864994));
#39198=CARTESIAN_POINT('Ctrl Pts',(-20.8707850578404,25.3409460126372,-4.69665999388323));
#39199=CARTESIAN_POINT('Ctrl Pts',(-20.8744470243656,25.3464130470483,-4.6962559145485));
#39200=CARTESIAN_POINT('Ctrl Pts',(-20.8762237310688,25.3490570467182,-4.6960601481742));
#39201=CARTESIAN_POINT('Ctrl Pts',(-20.8804647161472,25.3553480848593,-4.69559352825165));
#39202=CARTESIAN_POINT('Ctrl Pts',(-20.8829325472206,25.3589927109983,-4.69532254011838));
#39203=CARTESIAN_POINT('Ctrl Pts',(-20.8917332322331,25.3719328573335,-4.69435805126446));
#39204=CARTESIAN_POINT('Ctrl Pts',(-20.8981072182819,25.3812001840885,-4.6936629868024));
#39205=CARTESIAN_POINT('Ctrl Pts',(-20.9924683148742,25.5168679688499,-4.68342330206693));
#39206=CARTESIAN_POINT('Ctrl Pts',(-21.0893429300488,25.6368161151319,-4.67353061019756));
#39207=CARTESIAN_POINT('Ctrl Pts',(-21.3509961588839,25.9171174288147,-4.64820327432532));
#39208=CARTESIAN_POINT('Ctrl Pts',(-21.5250519611933,26.0676571186219,-4.63246638691006));
#39209=CARTESIAN_POINT('Ctrl Pts',(-21.785709120985,26.2484384182394,-4.61124474181449));
#39210=CARTESIAN_POINT('Ctrl Pts',(-21.859847220844,26.2954944066382,-4.60544623001482));
#39211=CARTESIAN_POINT('Ctrl Pts',(-21.9688630818831,26.3585941492496,-4.59734582894304));
#39212=CARTESIAN_POINT('Ctrl Pts',(-22.0022456392596,26.3771324753666,-4.59492029370877));
#39213=CARTESIAN_POINT('Ctrl Pts',(-22.0401442256527,26.3973059252628,-4.59223450943404));
#39214=CARTESIAN_POINT('Ctrl Pts',(-22.0443418622225,26.3995284358611,-4.59193795819502));
#39215=CARTESIAN_POINT('Ctrl Pts',(-22.0506536488911,26.402852474883,-4.59149345415158));
#39216=CARTESIAN_POINT('Ctrl Pts',(-22.0527641090184,26.4039609381761,-4.59134506170654));
#39217=CARTESIAN_POINT('Ctrl Pts',(-22.0563790721916,26.4058544873845,-4.59109128889231));
#39218=CARTESIAN_POINT('Ctrl Pts',(-22.0578829648923,26.4066407263354,-4.59098583466185));
#39219=CARTESIAN_POINT('Ctrl Pts',(-22.0609832742274,26.4082584591111,-4.59076868628164));
#39220=CARTESIAN_POINT('Ctrl Pts',(-22.0625797626786,26.4090898014168,-4.59065700193718));
#39221=CARTESIAN_POINT('Ctrl Pts',(-22.0664411735423,26.4110964503846,-4.59038719657879));
#39222=CARTESIAN_POINT('Ctrl Pts',(-22.0687068014021,26.4122704077472,-4.59022916171983));
#39223=CARTESIAN_POINT('Ctrl Pts',(-22.0723273939412,26.4141410020936,-4.58997704018022));
#39224=CARTESIAN_POINT('Ctrl Pts',(-22.0736814559545,26.4148393678708,-4.58988284461916));
#39225=CARTESIAN_POINT('Ctrl Pts',(-22.075036015346,26.4155367745563,-4.58978870905188));
#39226=CARTESIAN_POINT('Origin',(-23.5502525316942,23.5502525316942,-77.3107734492734));
#39227=CARTESIAN_POINT('',(-22.0750359182337,26.4155367245571,-3.09374624221682));
#39228=CARTESIAN_POINT('',(-22.0750361667496,26.4155368525077,-3.34376876818698));
#39229=CARTESIAN_POINT('',(-22.0750360153461,26.4155367745563,-77.3107734492734));
#39230=CARTESIAN_POINT('',(-26.7730016161112,23.552681809173,-3.93718354728755));
#39231=CARTESIAN_POINT('Ctrl Pts',(-22.0750359182355,26.4155367245581,-3.0937462422167));
#39232=CARTESIAN_POINT('Ctrl Pts',(-22.0146133082446,26.3844276156225,-3.09773139462589));
#39233=CARTESIAN_POINT('Ctrl Pts',(-21.95512803832,26.3513832493889,-3.10177819823092));
#39234=CARTESIAN_POINT('Ctrl Pts',(-21.879463016644,26.3061520264815,-3.10711032437475));
#39235=CARTESIAN_POINT('Ctrl Pts',(-21.8623488067689,26.2957034265546,-3.10832890551739));
#39236=CARTESIAN_POINT('Ctrl Pts',(-21.8400613104548,26.2818092578009,-3.10993276080145));
#39237=CARTESIAN_POINT('Ctrl Pts',(-21.834798655112,26.2785073140795,-3.11031271969719));
#39238=CARTESIAN_POINT('Ctrl Pts',(-21.8266930875078,26.2733889194499,-3.11089987464221));
#39239=CARTESIAN_POINT('Ctrl Pts',(-21.8238434043007,26.2715831747213,-3.11110667282468));
#39240=CARTESIAN_POINT('Ctrl Pts',(-21.818175141691,26.267978908031,-3.11151875488951));
#39241=CARTESIAN_POINT('Ctrl Pts',(-21.8153565151765,26.2661804676553,-3.11172403556082));
#39242=CARTESIAN_POINT('Ctrl Pts',(-21.8091851600086,26.2622292729161,-3.11217430293987));
#39243=CARTESIAN_POINT('Ctrl Pts',(-21.805833618262,26.2600746830372,-3.11241935795831));
#39244=CARTESIAN_POINT('Ctrl Pts',(-21.7962801454155,26.2539080185247,-3.11311938189167));
#39245=CARTESIAN_POINT('Ctrl Pts',(-21.7900880304783,26.2498808487965,-3.11357491540667));
#39246=CARTESIAN_POINT('Ctrl Pts',(-21.7762252664494,26.2407969438803,-3.11459885101972));
#39247=CARTESIAN_POINT('Ctrl Pts',(-21.7685623096419,26.2357286387576,-3.11516768640381));
#39248=CARTESIAN_POINT('Ctrl Pts',(-21.627106895636,26.1412976014961,-3.12572112375304));
#39249=CARTESIAN_POINT('Ctrl Pts',(-21.5001915959202,26.0420870881447,-3.13608712839143));
#39250=CARTESIAN_POINT('Ctrl Pts',(-21.1487327651533,25.7222642416072,-3.16757106908893));
#39251=CARTESIAN_POINT('Ctrl Pts',(-20.9484621960914,25.477842528873,-3.18949428733414));
#39252=CARTESIAN_POINT('Ctrl Pts',(-20.7844139327084,25.2044215027958,-3.20991184700231));
#39253=CARTESIAN_POINT('Ctrl Pts',(-20.7820882678076,25.2005266753592,-3.2102018854314));
#39254=CARTESIAN_POINT('Ctrl Pts',(-20.7770892269645,25.1921144021374,-3.21082657022639));
#39255=CARTESIAN_POINT('Ctrl Pts',(-20.7744186424213,25.1875952985944,-3.2111610639708));
#39256=CARTESIAN_POINT('Ctrl Pts',(-20.7672855715749,25.1754572641211,-3.2120565351764));
#39257=CARTESIAN_POINT('Ctrl Pts',(-20.762843297079,25.1678264206413,-3.21261637659596));
#39258=CARTESIAN_POINT('Ctrl Pts',(-20.7511616381436,25.1475688961617,-3.21409415249107));
#39259=CARTESIAN_POINT('Ctrl Pts',(-20.7439762248941,25.1349110777381,-3.21500890636815));
#39260=CARTESIAN_POINT('Ctrl Pts',(-20.7350311059628,25.1189016966401,-3.21615461940451));
#39261=CARTESIAN_POINT('Ctrl Pts',(-20.7331913672111,25.1155953933362,-3.21639063419207));
#39262=CARTESIAN_POINT('Ctrl Pts',(-20.7303002054151,25.1103779106149,-3.21676211907669));
#39263=CARTESIAN_POINT('Ctrl Pts',(-20.7292449000755,25.1084689039789,-3.21689783901887));
#39264=CARTESIAN_POINT('Ctrl Pts',(-20.7272912516306,25.1049263396863,-3.2171493205975));
#39265=CARTESIAN_POINT('Ctrl Pts',(-20.7263923932336,25.1032930837859,-3.21726511511223));
#39266=CARTESIAN_POINT('Ctrl Pts',(-20.7243966665359,25.0996593204121,-3.21752241317762));
#39267=CARTESIAN_POINT('Ctrl Pts',(-20.7233005077514,25.0976584325419,-3.21766387048355));
#39268=CARTESIAN_POINT('Ctrl Pts',(-20.7201201376017,25.0918384436021,-3.21807469137683));
#39269=CARTESIAN_POINT('Ctrl Pts',(-20.7180415236932,25.0880162647072,-3.21834369531924));
#39270=CARTESIAN_POINT('Ctrl Pts',(-20.7035197927782,25.0611842174393,-3.22022663717745));
#39271=CARTESIAN_POINT('Ctrl Pts',(-20.6913490266913,25.0380269435037,-3.22182342936607));
#39272=CARTESIAN_POINT('Ctrl Pts',(-20.6572660754931,24.9712143752057,-3.22635728895278));
#39273=CARTESIAN_POINT('Ctrl Pts',(-20.6360617185373,24.9272041099921,-3.22925544303751));
#39274=CARTESIAN_POINT('Ctrl Pts',(-20.5978124873225,24.8429712576515,-3.23466833505986));
#39275=CARTESIAN_POINT('Ctrl Pts',(-20.580569210251,24.8028518967939,-3.23719052580586));
#39276=CARTESIAN_POINT('Ctrl Pts',(-20.4372565046046,24.4498012524041,-3.25900292560566));
#39277=CARTESIAN_POINT('Ctrl Pts',(-20.3602356242372,24.1192378336382,-3.27707850944475));
#39278=CARTESIAN_POINT('Ctrl Pts',(-20.3349082663448,23.7690379877467,-3.29789718906894));
#39279=CARTESIAN_POINT('Ctrl Pts',(-20.3340059498439,23.755346990209,-3.29871323895835));
#39280=CARTESIAN_POINT('Ctrl Pts',(-20.3327820150424,23.7347748422324,-3.29994286698378));
#39281=CARTESIAN_POINT('Ctrl Pts',(-20.3323949795844,23.7278976325604,-3.3003545029345));
#39282=CARTESIAN_POINT('Ctrl Pts',(-20.3318858803563,23.7183032900765,-3.30092959730288));
#39283=CARTESIAN_POINT('Ctrl Pts',(-20.3317452022062,23.7155871312244,-3.30109249865328));
#39284=CARTESIAN_POINT('Ctrl Pts',(-20.3313007998519,23.7067912363577,-3.30162033290429));
#39285=CARTESIAN_POINT('Ctrl Pts',(-20.33101086416,23.7007108423363,-3.30198567841849));
#39286=CARTESIAN_POINT('Ctrl Pts',(-20.3301520313107,23.6815594429559,-3.3031379071427));
#39287=CARTESIAN_POINT('Ctrl Pts',(-20.3296455078209,23.668485892618,-3.30392666898512));
#39288=CARTESIAN_POINT('Ctrl Pts',(-20.3285546351352,23.6350717582092,-3.30594850691942));
#39289=CARTESIAN_POINT('Ctrl Pts',(-20.3280833113431,23.6147282928021,-3.30718502200711));
#39290=CARTESIAN_POINT('Ctrl Pts',(-20.3277191156577,23.5881338330159,-3.30880917625656));
#39291=CARTESIAN_POINT('Ctrl Pts',(-20.3276517229676,23.5818853815036,-3.30919133088));
#39292=CARTESIAN_POINT('Ctrl Pts',(-20.3275758739647,23.5722560035519,-3.30978112991998));
#39293=CARTESIAN_POINT('Ctrl Pts',(-20.32755456411,23.5688751694983,-3.30998837062342));
#39294=CARTESIAN_POINT('Ctrl Pts',(-20.3275227640037,23.5621513746698,-3.31040086059076));
#39295=CARTESIAN_POINT('Ctrl Pts',(-20.3275121551373,23.5588084184645,-3.31060610587258));
#39296=CARTESIAN_POINT('Ctrl Pts',(-20.3275003209145,23.5514922467953,-3.31105564982359));
#39297=CARTESIAN_POINT('Ctrl Pts',(-20.3275012417615,23.5475190375955,-3.31130001556216));
#39298=CARTESIAN_POINT('Ctrl Pts',(-20.3275247463536,23.5362244341546,-3.31199533357431));
#39299=CARTESIAN_POINT('Ctrl Pts',(-20.3275649315981,23.5289031360081,-3.31244683776656));
#39300=CARTESIAN_POINT('Ctrl Pts',(-20.3277109917855,23.5124856427681,-3.31346110224683));
#39301=CARTESIAN_POINT('Ctrl Pts',(-20.3278304329106,23.5033896585709,-3.31402428567378));
#39302=CARTESIAN_POINT('Ctrl Pts',(-20.3283225417495,23.475052329362,-3.31578272725679));
#39303=CARTESIAN_POINT('Ctrl Pts',(-20.3288290466735,23.4558140080136,-3.31698217247114));
#39304=CARTESIAN_POINT('Ctrl Pts',(-20.3313671587614,23.3838992385282,-3.32148745558336));
#39305=CARTESIAN_POINT('Ctrl Pts',(-20.3345187272752,23.3312730004496,-3.32482797106629));
#39306=CARTESIAN_POINT('Ctrl Pts',(-20.3474770468649,23.1780037861943,-3.33468856151785));
#39307=CARTESIAN_POINT('Ctrl Pts',(-20.3607302291696,23.0777229822386,-3.34130845058533));
#39308=CARTESIAN_POINT('Ctrl Pts',(-20.4352670071636,22.6644476900113,-3.36922967613078));
#39309=CARTESIAN_POINT('Ctrl Pts',(-20.5381086912875,22.3608119369038,-3.39148629748535));
#39310=CARTESIAN_POINT('Ctrl Pts',(-20.6913116872759,22.0626901771717,-3.41270112515197));
#39311=CARTESIAN_POINT('Ctrl Pts',(-20.6988901774037,22.0482148284786,-3.4137289867691));
#39312=CARTESIAN_POINT('Ctrl Pts',(-20.7082709259173,22.0306239423479,-3.41497476906555));
#39313=CARTESIAN_POINT('Ctrl Pts',(-20.7099685574379,22.0274533187226,-3.41519918000799));
#39314=CARTESIAN_POINT('Ctrl Pts',(-20.7127739886504,22.0222346974916,-3.41556831866835));
#39315=CARTESIAN_POINT('Ctrl Pts',(-20.7138787003547,22.0201850583981,-3.41571324218781));
#39316=CARTESIAN_POINT('Ctrl Pts',(-20.7158732940226,22.0164939503574,-3.41597412263115));
#39317=CARTESIAN_POINT('Ctrl Pts',(-20.7167623791621,22.0148520613506,-3.41609013013811));
#39318=CARTESIAN_POINT('Ctrl Pts',(-20.718675903383,22.0113256454033,-3.41633920652058));
#39319=CARTESIAN_POINT('Ctrl Pts',(-20.7197007942789,22.0094413734963,-3.41647224546646));
#39320=CARTESIAN_POINT('Ctrl Pts',(-20.7225093737042,22.0042900320959,-3.41683582226988));
#39321=CARTESIAN_POINT('Ctrl Pts',(-20.724296849491,22.0010250144202,-3.41706611712103));
#39322=CARTESIAN_POINT('Ctrl Pts',(-20.7335612041514,21.9841720538984,-3.41825410245119));
#39323=CARTESIAN_POINT('Ctrl Pts',(-20.7411306077314,21.9706348131623,-3.41920593085081));
#39324=CARTESIAN_POINT('Ctrl Pts',(-20.7857276633813,21.8922112162942,-3.42470898596819));
#39325=CARTESIAN_POINT('Ctrl Pts',(-20.8249079685812,21.8285679748215,-3.42913075517134));
#39326=CARTESIAN_POINT('Ctrl Pts',(-20.8896091848416,21.7312218711983,-3.43591656849854));
#39327=CARTESIAN_POINT('Ctrl Pts',(-20.9136375557161,21.6965650566027,-3.43833708242893));
#39328=CARTESIAN_POINT('Ctrl Pts',(-21.1016072789672,21.4365036556913,-3.45661451012401));
#39329=CARTESIAN_POINT('Ctrl Pts',(-21.2934811807223,21.2327562144385,-3.47171171900096));
#39330=CARTESIAN_POINT('Ctrl Pts',(-21.5878872878923,20.9918187389081,-3.49382923461142));
#39331=CARTESIAN_POINT('Ctrl Pts',(-21.6695898250489,20.9311753419974,-3.49986232380336));
#39332=CARTESIAN_POINT('Ctrl Pts',(-21.7618346328459,20.869251291161,-3.50662448700155));
#39333=CARTESIAN_POINT('Ctrl Pts',(-21.7696757563003,20.8640372431082,-3.5071988954544));
#39334=CARTESIAN_POINT('Ctrl Pts',(-21.7813326589687,20.8563593126052,-3.50805228764202));
#39335=CARTESIAN_POINT('Ctrl Pts',(-21.78513102622,20.8538689791287,-3.50833027770117));
#39336=CARTESIAN_POINT('Ctrl Pts',(-21.791633664599,20.8496252656295,-3.50880604434361));
#39337=CARTESIAN_POINT('Ctrl Pts',(-21.7943353326222,20.8478678921942,-3.50900367111503));
#39338=CARTESIAN_POINT('Ctrl Pts',(-21.7997582040599,20.8443520034477,-3.50940027325574));
#39339=CARTESIAN_POINT('Ctrl Pts',(-21.8024794316459,20.8425935335055,-3.50959924996803));
#39340=CARTESIAN_POINT('Ctrl Pts',(-21.8087625460157,20.8385467741265,-3.51005858173033));
#39341=CARTESIAN_POINT('Ctrl Pts',(-21.8123262934419,20.8362613975957,-3.51031904497681));
#39342=CARTESIAN_POINT('Ctrl Pts',(-21.823101247575,20.8293815102322,-3.51110635732045));
#39343=CARTESIAN_POINT('Ctrl Pts',(-21.8303262030297,20.8248086971283,-3.51163401189023));
#39344=CARTESIAN_POINT('Ctrl Pts',(-21.8468849982811,20.8144203824624,-3.51284277622807));
#39345=CARTESIAN_POINT('Ctrl Pts',(-21.8562305402623,20.8086238204403,-3.5135245801558));
#39346=CARTESIAN_POINT('Ctrl Pts',(-21.8867866361249,20.7898873194417,-3.51575259289498));
#39347=CARTESIAN_POINT('Ctrl Pts',(-21.9081167897839,20.777145061713,-3.51730601536662));
#39348=CARTESIAN_POINT('Ctrl Pts',(-21.9935337498009,20.7274495393203,-3.523520494314));
#39349=CARTESIAN_POINT('Ctrl Pts',(-22.0587331900814,20.6924633987414,-3.52825097890112));
#39350=CARTESIAN_POINT('Ctrl Pts',(-22.2307490273806,20.6076499521125,-3.54070189462505));
#39351=CARTESIAN_POINT('Ctrl Pts',(-22.3391920540689,20.5613852669244,-3.54852587884169));
#39352=CARTESIAN_POINT('Ctrl Pts',(-22.6902340144543,20.4338668914472,-3.57363499264321));
#39353=CARTESIAN_POINT('Ctrl Pts',(-22.9400928691539,20.3754756776395,-3.59125660907819));
#39354=CARTESIAN_POINT('Ctrl Pts',(-23.1971128654555,20.3469076653475,-3.60780299921877));
#39355=CARTESIAN_POINT('Ctrl Pts',(-23.1999928352131,20.3465914850515,-3.60798819783091));
#39356=CARTESIAN_POINT('Ctrl Pts',(-23.2101054723464,20.3454950587212,-3.60863776074529));
#39357=CARTESIAN_POINT('Ctrl Pts',(-23.2173404156002,20.3447354115217,-3.60910115674214));
#39358=CARTESIAN_POINT('Ctrl Pts',(-23.2255919180676,20.3438972664085,-3.60962810657254));
#39359=CARTESIAN_POINT('Ctrl Pts',(-23.2266059376766,20.3437947534865,-3.60969283617012));
#39360=CARTESIAN_POINT('Ctrl Pts',(-23.2475368661123,20.3416887586883,-3.61102839964508));
#39361=CARTESIAN_POINT('Ctrl Pts',(-23.2674725764781,20.3398703417643,-3.61229008565064));
#39362=CARTESIAN_POINT('Ctrl Pts',(-23.2912750506689,20.3379226680949,-3.61378308714745));
#39363=CARTESIAN_POINT('Ctrl Pts',(-23.2951261556685,20.337614515843,-3.61402422814353));
#39364=CARTESIAN_POINT('Ctrl Pts',(-23.3013810731477,20.3371253368053,-3.61441519715343));
#39365=CARTESIAN_POINT('Ctrl Pts',(-23.3037845350202,20.3369400818839,-3.61456526240293));
#39366=CARTESIAN_POINT('Ctrl Pts',(-23.3080581077314,20.3366155048692,-3.61483179555489));
#39367=CARTESIAN_POINT('Ctrl Pts',(-23.3099281311343,20.3364751184709,-3.61494832372249));
#39368=CARTESIAN_POINT('Ctrl Pts',(-23.3138852191887,20.3361815251161,-3.61519469025364));
#39369=CARTESIAN_POINT('Ctrl Pts',(-23.3159723054859,20.3360287191051,-3.61532450541527));
#39370=CARTESIAN_POINT('Ctrl Pts',(-23.3215385056725,20.335626640068,-3.61567038658308));
#39371=CARTESIAN_POINT('Ctrl Pts',(-23.3250178903064,20.33538098132,-3.61588624792674));
#39372=CARTESIAN_POINT('Ctrl Pts',(-23.3412907449379,20.334258599004,-3.61689422781572));
#39373=CARTESIAN_POINT('Ctrl Pts',(-23.3540892090944,20.3334525740801,-3.61768240206108));
#39374=CARTESIAN_POINT('Ctrl Pts',(-23.6611964437418,20.3159511889739,-3.63649228160364));
#39375=CARTESIAN_POINT('Ctrl Pts',(-23.9564674332818,20.3396340472565,-3.65240117808815));
#39376=CARTESIAN_POINT('Ctrl Pts',(-24.3476659219888,20.4259248960626,-3.67494596206755));
#39377=CARTESIAN_POINT('Ctrl Pts',(-24.4497018342685,20.4537577470525,-3.6809568410531));
#39378=CARTESIAN_POINT('Ctrl Pts',(-24.645272535807,20.5175879495613,-3.69292569721338));
#39379=CARTESIAN_POINT('Ctrl Pts',(-24.7388593186507,20.5530314768552,-3.69886238225315));
#39380=CARTESIAN_POINT('Ctrl Pts',(-24.8392460979695,20.5964920316765,-3.70552057819909));
#39381=CARTESIAN_POINT('Ctrl Pts',(-24.8478356248044,20.60025530815,-3.70609263808224));
#39382=CARTESIAN_POINT('Ctrl Pts',(-24.8605520787762,20.6058929743546,-3.70694309492361));
#39383=CARTESIAN_POINT('Ctrl Pts',(-24.8646917274236,20.6077386903727,-3.70722050756741));
#39384=CARTESIAN_POINT('Ctrl Pts',(-24.8717659533681,20.6109107329723,-3.70769553968746));
#39385=CARTESIAN_POINT('Ctrl Pts',(-24.8747024701196,20.6122327404283,-3.70789301036694));
#39386=CARTESIAN_POINT('Ctrl Pts',(-24.8805877349573,20.6148928782297,-3.70828934730965));
#39387=CARTESIAN_POINT('Ctrl Pts',(-24.8835364569966,20.6162310555221,-3.7084882149881));
#39388=CARTESIAN_POINT('Ctrl Pts',(-24.8894590481103,20.6189295942829,-3.70888822992542));
#39389=CARTESIAN_POINT('Ctrl Pts',(-24.8924328730145,20.6202900424715,-3.70908937998969));
#39390=CARTESIAN_POINT('Ctrl Pts',(-24.9018905781676,20.6246341190074,-3.70973004810133));
#39391=CARTESIAN_POINT('Ctrl Pts',(-24.9083665861363,20.627634746362,-3.71017015381869));
#39392=CARTESIAN_POINT('Ctrl Pts',(-24.9461944677564,20.6453149925964,-3.71274928837823));
#39393=CARTESIAN_POINT('Ctrl Pts',(-24.9773171476909,20.6604770342075,-3.71490501928254));
#39394=CARTESIAN_POINT('Ctrl Pts',(-25.0668504056003,20.7058940556585,-3.72120790096503));
#39395=CARTESIAN_POINT('Ctrl Pts',(-25.1245837032092,20.7374381753716,-3.72539967381491));
#39396=CARTESIAN_POINT('Ctrl Pts',(-25.2500102038357,20.8110397494385,-3.7347965314476));
#39397=CARTESIAN_POINT('Ctrl Pts',(-25.3171892415055,20.8538853576992,-3.74002578551684));
#39398=CARTESIAN_POINT('Ctrl Pts',(-25.6473207923854,21.0820759649078,-3.76669041093025));
#39399=CARTESIAN_POINT('Ctrl Pts',(-25.8830427121671,21.3035497250365,-3.7891568339535));
#39400=CARTESIAN_POINT('Ctrl Pts',(-26.0919767670113,21.5688358196982,-3.81052410863379));
#39401=CARTESIAN_POINT('Ctrl Pts',(-26.1017964136027,21.5814970570262,-3.81153190292591));
#39402=CARTESIAN_POINT('Ctrl Pts',(-26.1136888918762,21.5970694009323,-3.81275628041603));
#39403=CARTESIAN_POINT('Ctrl Pts',(-26.1158516133871,21.5999111084258,-3.81297909889448));
#39404=CARTESIAN_POINT('Ctrl Pts',(-26.119411874759,21.6046052828185,-3.81334615421583));
#39405=CARTESIAN_POINT('Ctrl Pts',(-26.120812137393,21.6064556645459,-3.81349058309648));
#39406=CARTESIAN_POINT('Ctrl Pts',(-26.1233351498344,21.6097972019338,-3.81375093165768));
#39407=CARTESIAN_POINT('Ctrl Pts',(-26.1244585998637,21.611287816897,-3.81386690098521));
#39408=CARTESIAN_POINT('Ctrl Pts',(-26.1268737377152,21.6144980667079,-3.81411629420121));
#39409=CARTESIAN_POINT('Ctrl Pts',(-26.1281649957672,21.6162180139894,-3.81424968744386));
#39410=CARTESIAN_POINT('Ctrl Pts',(-26.1317018685611,21.6209389407278,-3.81461521773985));
#39411=CARTESIAN_POINT('Ctrl Pts',(-26.1339439802461,21.6239425592036,-3.81484710738031));
#39412=CARTESIAN_POINT('Ctrl Pts',(-26.1456332589118,21.6396590873752,-3.81605700183655));
#39413=CARTESIAN_POINT('Ctrl Pts',(-26.1549920669126,21.6524378920063,-3.81702888344381));
#39414=CARTESIAN_POINT('Ctrl Pts',(-26.247794629572,21.7811331219167,-3.82670425956788));
#39415=CARTESIAN_POINT('Ctrl Pts',(-26.3235509252817,21.9024224874691,-3.83491801903236));
#39416=CARTESIAN_POINT('Ctrl Pts',(-26.4900429549156,22.2131951527951,-3.85482929947714));
#39417=CARTESIAN_POINT('Ctrl Pts',(-26.5707907319383,22.4072564477704,-3.86633771881029));
#39418=CARTESIAN_POINT('Ctrl Pts',(-26.6377133469624,22.6260936063406,-3.87943350280407));
#39419=CARTESIAN_POINT('Ctrl Pts',(-26.6431481818419,22.6444487526349,-3.88053246862601));
#39420=CARTESIAN_POINT('Ctrl Pts',(-26.6628868599382,22.7133619924785,-3.88466255817534));
#39421=CARTESIAN_POINT('Ctrl Pts',(-26.6761166333174,22.7642172531722,-3.88771877644782));
#39422=CARTESIAN_POINT('Ctrl Pts',(-26.7049169487885,22.8871907650272,-3.89515260637662));
#39423=CARTESIAN_POINT('Ctrl Pts',(-26.7192652026212,22.9595615236503,-3.89956336771272));
#39424=CARTESIAN_POINT('Ctrl Pts',(-26.7325085047014,23.0409005732024,-3.90458222000383));
#39425=CARTESIAN_POINT('Ctrl Pts',(-26.7338651442123,23.0494499493567,-3.90511048440937));
#39426=CARTESIAN_POINT('Ctrl Pts',(-26.7358521422731,23.062306193363,-3.9059060205549));
#39427=CARTESIAN_POINT('Ctrl Pts',(-26.7365082541625,23.0666090899459,-3.90617247456588));
#39428=CARTESIAN_POINT('Ctrl Pts',(-26.7376275223649,23.0740505822616,-3.90663362328748));
#39429=CARTESIAN_POINT('Ctrl Pts',(-26.7380947660825,23.0771885652604,-3.90682818807761));
#39430=CARTESIAN_POINT('Ctrl Pts',(-26.7390247983188,23.0834985601429,-3.90721963910655));
#39431=CARTESIAN_POINT('Ctrl Pts',(-26.7394874892114,23.0866705821023,-3.90741652817207));
#39432=CARTESIAN_POINT('Ctrl Pts',(-26.7404176493971,23.0931146866533,-3.90781673732065));
#39433=CARTESIAN_POINT('Ctrl Pts',(-26.7408848188975,23.0963868078259,-3.90802006664926));
#39434=CARTESIAN_POINT('Ctrl Pts',(-26.7419493485436,23.1039257961634,-3.90848880665395));
#39435=CARTESIAN_POINT('Ctrl Pts',(-26.7425431866619,23.1081931471619,-3.90875432871478));
#39436=CARTESIAN_POINT('Ctrl Pts',(-26.7440489305974,23.1191747684734,-3.90943813860956));
#39437=CARTESIAN_POINT('Ctrl Pts',(-26.744948218134,23.125890722023,-3.90985682567316));
#39438=CARTESIAN_POINT('Ctrl Pts',(-26.7640325227331,23.2719132513757,-3.91897110692897));
#39439=CARTESIAN_POINT('Ctrl Pts',(-26.7731074835901,23.4122349794034,-3.92795586024967));
#39440=CARTESIAN_POINT('Ctrl Pts',(-26.7730016161112,23.552681809173,-3.93718354728755));
#39441=CARTESIAN_POINT('Ctrl Pts',(-26.7730016191972,23.5526777117792,-3.93718327807921));
#39442=CARTESIAN_POINT('Ctrl Pts',(-26.7728336327151,23.7759099102419,-3.95185015161121));
#39443=CARTESIAN_POINT('Ctrl Pts',(-26.7494711541764,23.9985172774985,-3.96710418728231));
#39444=CARTESIAN_POINT('Ctrl Pts',(-26.6831336232011,24.3122736075055,-3.9886734987549));
#39445=CARTESIAN_POINT('Ctrl Pts',(-26.6586505654969,24.4066897277443,-3.99516388714361));
#39446=CARTESIAN_POINT('Ctrl Pts',(-26.6198690538734,24.5324623615074,-4.00369214877209));
#39447=CARTESIAN_POINT('Ctrl Pts',(-26.6092977090653,24.5649074278942,-4.00588116977758));
#39448=CARTESIAN_POINT('Ctrl Pts',(-26.5923670199883,24.6141983959673,-4.00918351284334));
#39449=CARTESIAN_POINT('Ctrl Pts',(-26.5863788383415,24.6311680916985,-4.0103161718275));
#39450=CARTESIAN_POINT('Ctrl Pts',(-26.5789185356788,24.6517583398107,-4.01168452098841));
#39451=CARTESIAN_POINT('Ctrl Pts',(-26.5775817221573,24.6554270798815,-4.01192809984516));
#39452=CARTESIAN_POINT('Ctrl Pts',(-26.575486360734,24.6611452436578,-4.01230737459805));
#39453=CARTESIAN_POINT('Ctrl Pts',(-26.5747323962068,24.663196325013,-4.01244334418726));
#39454=CARTESIAN_POINT('Ctrl Pts',(-26.5733960723866,24.6668202671541,-4.01268344726817));
#39455=CARTESIAN_POINT('Ctrl Pts',(-26.5728145744723,24.6683934320668,-4.01278763193865));
#39456=CARTESIAN_POINT('Ctrl Pts',(-26.571569606587,24.6717534583432,-4.01301005793523));
#39457=CARTESIAN_POINT('Ctrl Pts',(-26.5709057813275,24.6735401800909,-4.01312827715612));
#39458=CARTESIAN_POINT('Ctrl Pts',(-26.56898398563,24.6786987747581,-4.01346943416195));
#39459=CARTESIAN_POINT('Ctrl Pts',(-26.5677219465601,24.682069144541,-4.01369212714684));
#39460=CARTESIAN_POINT('Ctrl Pts',(-26.5620998063961,24.697007247705,-4.01467827671479));
#39461=CARTESIAN_POINT('Ctrl Pts',(-26.5576787376439,24.7085521527988,-4.01543811386994));
#39462=CARTESIAN_POINT('Ctrl Pts',(-26.552136447766,24.7227792739579,-4.01637196251905));
#39463=CARTESIAN_POINT('Ctrl Pts',(-26.5510779664004,24.7254855798491,-4.01654948769521));
#39464=CARTESIAN_POINT('Ctrl Pts',(-26.4255609228959,25.0451301122219,-4.03750422129371));
#39465=CARTESIAN_POINT('Ctrl Pts',(-26.2516423830581,25.3404052804288,-4.05553471311839));
#39466=CARTESIAN_POINT('Ctrl Pts',(-25.993266798087,25.6531133875712,-4.07864825391055));
#39467=CARTESIAN_POINT('Ctrl Pts',(-25.9503603187814,25.7019552149541,-4.08238877604869));
#39468=CARTESIAN_POINT('Ctrl Pts',(-25.8453083372892,25.8144849659556,-4.09137260309972));
#39469=CARTESIAN_POINT('Ctrl Pts',(-25.7819476879176,25.8769592539073,-4.09665841262858));
#39470=CARTESIAN_POINT('Ctrl Pts',(-25.7065369247427,25.9453979466044,-4.1028460980298));
#39471=CARTESIAN_POINT('Ctrl Pts',(-25.6969333744224,25.9540090281287,-4.10363223842742));
#39472=CARTESIAN_POINT('Ctrl Pts',(-25.6843842381346,25.9651261045282,-4.10465719925248));
#39473=CARTESIAN_POINT('Ctrl Pts',(-25.6814853778949,25.9676848613109,-4.10489380754055));
#39474=CARTESIAN_POINT('Ctrl Pts',(-25.6761988332345,25.9723342721304,-4.10532501686365));
#39475=CARTESIAN_POINT('Ctrl Pts',(-25.6738126489147,25.9744266308095,-4.10551954644499));
#39476=CARTESIAN_POINT('Ctrl Pts',(-25.6691569182061,25.9784969235143,-4.10589889441023));
#39477=CARTESIAN_POINT('Ctrl Pts',(-25.6668876825266,25.9804752095058,-4.10608369787106));
#39478=CARTESIAN_POINT('Ctrl Pts',(-25.6617052249204,25.9849804341673,-4.10650553937267));
#39479=CARTESIAN_POINT('Ctrl Pts',(-25.6587902366496,25.9875053255973,-4.1067426620319));
#39480=CARTESIAN_POINT('Ctrl Pts',(-25.6509304698171,25.9942886090889,-4.10738162032149));
#39481=CARTESIAN_POINT('Ctrl Pts',(-25.6459772968533,25.9985372077518,-4.10778386033387));
#39482=CARTESIAN_POINT('Ctrl Pts',(-25.6231479266305,26.0179991249098,-4.10963587847788));
#39483=CARTESIAN_POINT('Ctrl Pts',(-25.6051191192121,26.0330315849323,-4.11109306572182));
#39484=CARTESIAN_POINT('Ctrl Pts',(-25.5776413846346,26.0554382717038,-4.11330637656465));
#39485=CARTESIAN_POINT('Ctrl Pts',(-25.5683126254925,26.0629591609153,-4.11405650155353));
#39486=CARTESIAN_POINT('Ctrl Pts',(-25.5550517343898,26.0735286701699,-4.11512102350802));
#39487=CARTESIAN_POINT('Ctrl Pts',(-25.5511540714221,26.0766205456614,-4.11543369294684));
#39488=CARTESIAN_POINT('Ctrl Pts',(-25.5458511497258,26.0808071925165,-4.11585880087854));
#39489=CARTESIAN_POINT('Ctrl Pts',(-25.5444521045998,26.0819098542997,-4.11597092770353));
#39490=CARTESIAN_POINT('Ctrl Pts',(-25.5394136428434,26.0858741656935,-4.11637463817346));
#39491=CARTESIAN_POINT('Ctrl Pts',(-25.5357689880651,26.0887291217053,-4.11666648442644));
#39492=CARTESIAN_POINT('Ctrl Pts',(-25.5305069230252,26.0928327729702,-4.11708758166432));
#39493=CARTESIAN_POINT('Ctrl Pts',(-25.5288944451092,26.0940878086254,-4.11721658482149));
#39494=CARTESIAN_POINT('Ctrl Pts',(-25.5218101597198,26.0995908906593,-4.11778319386628));
#39495=CARTESIAN_POINT('Ctrl Pts',(-25.5163258889227,26.1038227974034,-4.11822142543565));
#39496=CARTESIAN_POINT('Ctrl Pts',(-25.5068573150424,26.1110805842291,-4.11897733872554));
#39497=CARTESIAN_POINT('Ctrl Pts',(-25.5028795153936,26.1141149412143,-4.11929469295917));
#39498=CARTESIAN_POINT('Ctrl Pts',(-25.4957007129822,26.1195646997647,-4.11986705364709));
#39499=CARTESIAN_POINT('Ctrl Pts',(-25.4925022307709,26.1219834175526,-4.12012193320673));
#39500=CARTESIAN_POINT('Ctrl Pts',(-25.4856156562066,26.1271709252496,-4.12067042354279));
#39501=CARTESIAN_POINT('Ctrl Pts',(-25.4819261218426,26.1299377782967,-4.12096410651717));
#39502=CARTESIAN_POINT('Ctrl Pts',(-25.461684519251,26.1450495735585,-4.12257436355939));
#39503=CARTESIAN_POINT('Ctrl Pts',(-25.4450203319108,26.1572429198352,-4.12389655355184));
#39504=CARTESIAN_POINT('Ctrl Pts',(-25.407532310553,26.1841239599864,-4.12686330842022));
#39505=CARTESIAN_POINT('Ctrl Pts',(-25.3866492795549,26.1987263953671,-4.12851077996509));
#39506=CARTESIAN_POINT('Ctrl Pts',(-25.2862664408559,26.267160925678,-4.13640511988243));
#39507=CARTESIAN_POINT('Ctrl Pts',(-25.2045658889655,26.3176665511896,-4.14275875411517));
#39508=CARTESIAN_POINT('Ctrl Pts',(-24.862725719322,26.5084334380641,-4.1689722350157));
#39509=CARTESIAN_POINT('Ctrl Pts',(-24.5861379701052,26.616255291323,-4.18948368793534));
#39510=CARTESIAN_POINT('Ctrl Pts',(-24.2906713409112,26.6868057614825,-4.20864143254407));
#39511=CARTESIAN_POINT('Ctrl Pts',(-24.2826069971575,26.6886985033127,-4.2091621794511));
#39512=CARTESIAN_POINT('Ctrl Pts',(-24.2686036342257,26.6919282490206,-4.21006262182683));
#39513=CARTESIAN_POINT('Ctrl Pts',(-24.2626680033923,26.6932795466074,-4.21044310878972));
#39514=CARTESIAN_POINT('Ctrl Pts',(-24.2541751033628,26.6951877336779,-4.21098579338859));
#39515=CARTESIAN_POINT('Ctrl Pts',(-24.2516209760631,26.6957583283732,-4.21114877527473));
#39516=CARTESIAN_POINT('Ctrl Pts',(-24.2472048157776,26.696739256868,-4.21143018635761));
#39517=CARTESIAN_POINT('Ctrl Pts',(-24.2453431111723,26.6971510499783,-4.21154870025574));
#39518=CARTESIAN_POINT('Ctrl Pts',(-24.2417589335762,26.6979405035482,-4.21177663336352));
#39519=CARTESIAN_POINT('Ctrl Pts',(-24.2400365195256,26.6983184017432,-4.21188606636495));
#39520=CARTESIAN_POINT('Ctrl Pts',(-24.2359547161622,26.6992104399149,-4.21214516109982));
#39521=CARTESIAN_POINT('Ctrl Pts',(-24.2335950534028,26.6997233430598,-4.21229475108248));
#39522=CARTESIAN_POINT('Ctrl Pts',(-24.2253285333156,26.7015104502032,-4.21281814276097));
#39523=CARTESIAN_POINT('Ctrl Pts',(-24.2194186231444,26.7027707029954,-4.2131911442657));
#39524=CARTESIAN_POINT('Ctrl Pts',(-24.2014132749565,26.7065573219616,-4.21432404328435));
#39525=CARTESIAN_POINT('Ctrl Pts',(-24.189306652564,26.7090307899159,-4.21508098890193));
#39526=CARTESIAN_POINT('Ctrl Pts',(-23.8961781515021,26.7671647498285,-4.23329884765875));
#39527=CARTESIAN_POINT('Ctrl Pts',(-23.6089416045226,26.7851877217823,-4.24879961257162));
#39528=CARTESIAN_POINT('Ctrl Pts',(-23.2201739368802,26.7577134448672,-4.27071409289777));
#39529=CARTESIAN_POINT('Ctrl Pts',(-23.1176948338158,26.7455066969607,-4.27656964599048));
#39530=CARTESIAN_POINT('Ctrl Pts',(-22.9430996190028,26.7161560231207,-4.28684125176797));
#39531=CARTESIAN_POINT('Ctrl Pts',(-22.8706643773789,26.7014012601985,-4.29119110434243));
#39532=CARTESIAN_POINT('Ctrl Pts',(-22.7746610488359,26.6783816545602,-4.29710684683183));
#39533=CARTESIAN_POINT('Ctrl Pts',(-22.7505863152861,26.6723140057396,-4.29860308581414));
#39534=CARTESIAN_POINT('Ctrl Pts',(-22.7159585223496,26.6631598340035,-4.30077460580838));
#39535=CARTESIAN_POINT('Ctrl Pts',(-22.7053470008415,26.6602964230362,-4.30144270126641));
#39536=CARTESIAN_POINT('Ctrl Pts',(-22.6865217621372,26.6551131669631,-4.30263272039935));
#39537=CARTESIAN_POINT('Ctrl Pts',(-22.6783021842503,26.6528148592079,-4.30315394199495));
#39538=CARTESIAN_POINT('Ctrl Pts',(-22.6660160917138,26.6493268179649,-4.30393550318894));
#39539=CARTESIAN_POINT('Ctrl Pts',(-22.6619425900287,26.6481616589734,-4.30419504052507));
#39540=CARTESIAN_POINT('Ctrl Pts',(-22.6547591392241,26.646091616199,-4.30465344800714));
#39541=CARTESIAN_POINT('Ctrl Pts',(-22.6516482281152,26.6451900687973,-4.30485220887214));
#39542=CARTESIAN_POINT('Ctrl Pts',(-22.6454458940905,26.6433824819026,-4.30524896652729));
#39543=CARTESIAN_POINT('Ctrl Pts',(-22.6423544598315,26.6424764937171,-4.30544696145242));
#39544=CARTESIAN_POINT('Ctrl Pts',(-22.63491294079,26.6402835307959,-4.30592414076378));
#39545=CARTESIAN_POINT('Ctrl Pts',(-22.6305642133307,26.6389920057879,-4.30620347398674));
#39546=CARTESIAN_POINT('Ctrl Pts',(-22.6172186258811,26.6349978276751,-4.30706217593535));
#39547=CARTESIAN_POINT('Ctrl Pts',(-22.6082309047132,26.6322650335787,-4.30764253239619));
#39548=CARTESIAN_POINT('Ctrl Pts',(-22.5030125558045,26.5997692426221,-4.31446109410309));
#39549=CARTESIAN_POINT('Ctrl Pts',(-22.4082260683628,26.5655527880011,-4.3208458640486));
#39550=CARTESIAN_POINT('Ctrl Pts',(-22.2335879730295,26.4930947004337,-4.33308977919066));
#39551=CARTESIAN_POINT('Ctrl Pts',(-22.1534662401888,26.4559172684158,-4.33890733600597));
#39552=CARTESIAN_POINT('Ctrl Pts',(-22.0750357159536,26.4155366204114,-4.34479105736985));
#39553=CARTESIAN_POINT('Ctrl Pts',(-22.075036015346,26.4155367745563,-4.58978870905188));
#39554=CARTESIAN_POINT('Ctrl Pts',(-22.0797990834668,26.4179890816101,-4.589457698007));
#39555=CARTESIAN_POINT('Ctrl Pts',(-22.0845683014347,26.4204295299504,-4.58912742875724));
#39556=CARTESIAN_POINT('Ctrl Pts',(-22.1841440218444,26.4710703344603,-4.58225567891223));
#39557=CARTESIAN_POINT('Ctrl Pts',(-22.2812847583401,26.514566169619,-4.57600230409775));
#39558=CARTESIAN_POINT('Ctrl Pts',(-22.6088403691738,26.6421710623346,-4.55580530523899));
#39559=CARTESIAN_POINT('Ctrl Pts',(-22.8466846975347,26.7048083170721,-4.54248217815563));
#39560=CARTESIAN_POINT('Ctrl Pts',(-23.1988294621773,26.7556943264301,-4.52219936221725));
#39561=CARTESIAN_POINT('Ctrl Pts',(-23.3090489820097,26.7658664078369,-4.51578477715329));
#39562=CARTESIAN_POINT('Ctrl Pts',(-23.4688897361643,26.7723534718767,-4.50625409460115));
#39563=CARTESIAN_POINT('Ctrl Pts',(-23.5182504502743,26.7732216335089,-4.5032801468792));
#39564=CARTESIAN_POINT('Ctrl Pts',(-23.5754924223601,26.7729133345418,-4.49978960689193));
#39565=CARTESIAN_POINT('Ctrl Pts',(-23.5833749495089,26.7728419572942,-4.499308026359));
#39566=CARTESIAN_POINT('Ctrl Pts',(-23.5954040168434,26.772688893479,-4.49857169267415));
#39567=CARTESIAN_POINT('Ctrl Pts',(-23.5995508318443,26.7726281211795,-4.49831759641202));
#39568=CARTESIAN_POINT('Ctrl Pts',(-23.6067267313381,26.7725091021779,-4.49787744261328));
#39569=CARTESIAN_POINT('Ctrl Pts',(-23.6097558794429,26.7724545881699,-4.49769150251613));
#39570=CARTESIAN_POINT('Ctrl Pts',(-23.6160358822205,26.7723327116264,-4.49730572344989));
#39571=CARTESIAN_POINT('Ctrl Pts',(-23.6192867197137,26.7722647004907,-4.49710586431211));
#39572=CARTESIAN_POINT('Ctrl Pts',(-23.6271825093837,26.7720875567335,-4.49662004330929));
#39573=CARTESIAN_POINT('Ctrl Pts',(-23.6318273296969,26.7719732989266,-4.49633392073081));
#39574=CARTESIAN_POINT('Ctrl Pts',(-23.6492396578501,26.7715072941398,-4.49526006356324));
#39575=CARTESIAN_POINT('Ctrl Pts',(-23.662005153204,26.7710896961222,-4.49447026334825));
#39576=CARTESIAN_POINT('Ctrl Pts',(-23.8706145710358,26.7630237765639,-4.48152144685554));
#39577=CARTESIAN_POINT('Ctrl Pts',(-24.0653244861559,26.7376035150987,-4.46878868858443));
#39578=CARTESIAN_POINT('Ctrl Pts',(-24.3713388746256,26.6688724783629,-4.44781533513045));
#39579=CARTESIAN_POINT('Ctrl Pts',(-24.484684633235,26.6368053072332,-4.43983538719622));
#39580=CARTESIAN_POINT('Ctrl Pts',(-24.774942584346,26.5372298740477,-4.4190751410826));
#39581=CARTESIAN_POINT('Ctrl Pts',(-24.9481412767853,26.4602054204499,-4.40634864615721));
#39582=CARTESIAN_POINT('Ctrl Pts',(-25.120419607617,26.3646358994787,-4.39398056731649));
#39583=CARTESIAN_POINT('Ctrl Pts',(-25.1272258670839,26.3608278268348,-4.39349246757406));
#39584=CARTESIAN_POINT('Ctrl Pts',(-25.1365610677554,26.3555602358763,-4.39282381034444));
#39585=CARTESIAN_POINT('Ctrl Pts',(-25.1391018772499,26.3541219730222,-4.39264190035741));
#39586=CARTESIAN_POINT('Ctrl Pts',(-25.1433511688566,26.351708967859,-4.39233781282694));
#39587=CARTESIAN_POINT('Ctrl Pts',(-25.1450607129072,26.3507361143357,-4.39221551300868));
#39588=CARTESIAN_POINT('Ctrl Pts',(-25.1484269167665,26.3488164202625,-4.39197477414275));
#39589=CARTESIAN_POINT('Ctrl Pts',(-25.1500836263822,26.347869673478,-4.39185632929509));
#39590=CARTESIAN_POINT('Ctrl Pts',(-25.153735825363,26.3457782750215,-4.39159529856463));
#39591=CARTESIAN_POINT('Ctrl Pts',(-25.1557309354049,26.3446329549681,-4.39145275618068));
#39592=CARTESIAN_POINT('Ctrl Pts',(-25.1627026792051,26.3406207994701,-4.39095483152919));
#39593=CARTESIAN_POINT('Ctrl Pts',(-25.167672912484,26.337742775808,-4.39060017247096));
#39594=CARTESIAN_POINT('Ctrl Pts',(-25.2181198452733,26.3083510230434,-4.38700339913134));
#39595=CARTESIAN_POINT('Ctrl Pts',(-25.2629513524647,26.2807382393759,-4.38383139171528));
#39596=CARTESIAN_POINT('Ctrl Pts',(-25.5687756302272,26.081875882708,-4.3622194557549));
#39597=CARTESIAN_POINT('Ctrl Pts',(-25.8043812766291,25.874582329617,-4.34556050899947));
#39598=CARTESIAN_POINT('Ctrl Pts',(-26.0635865407976,25.5694210551125,-4.32265276985209));
#39599=CARTESIAN_POINT('Ctrl Pts',(-26.1178737533197,25.499921430596,-4.31753537093236));
#39600=CARTESIAN_POINT('Ctrl Pts',(-26.2042266936628,25.3794991066975,-4.308752083828));
#39601=CARTESIAN_POINT('Ctrl Pts',(-26.2378401991909,25.3297450685115,-4.30514591011375));
#39602=CARTESIAN_POINT('Ctrl Pts',(-26.2744901674349,25.2720874804144,-4.30098102958072));
#39603=CARTESIAN_POINT('Ctrl Pts',(-26.2789102603196,25.2650741797409,-4.30047466473154));
#39604=CARTESIAN_POINT('Ctrl Pts',(-26.285527976235,25.2544835697009,-4.29971034502765));
#39605=CARTESIAN_POINT('Ctrl Pts',(-26.2877457728553,25.2509188548589,-4.29945313705026));
#39606=CARTESIAN_POINT('Ctrl Pts',(-26.2915555595553,25.2447685368471,-4.29900945985568));
#39607=CARTESIAN_POINT('Ctrl Pts',(-26.2931508765982,25.2421849924323,-4.29882311370921));
#39608=CARTESIAN_POINT('Ctrl Pts',(-26.2964357599669,25.2368484148579,-4.29843825223085));
#39609=CARTESIAN_POINT('Ctrl Pts',(-26.2981248427757,25.2340950891277,-4.29823971935126));
#39610=CARTESIAN_POINT('Ctrl Pts',(-26.3026766331881,25.2266502569967,-4.29770297759967));
#39611=CARTESIAN_POINT('Ctrl Pts',(-26.3055314742636,25.2219539751102,-4.29736448018439));
#39612=CARTESIAN_POINT('Ctrl Pts',(-26.3160444717676,25.2045597558923,-4.29611104044488));
#39613=CARTESIAN_POINT('Ctrl Pts',(-26.3236268839384,25.1918164623113,-4.29519333112648));
#39614=CARTESIAN_POINT('Ctrl Pts',(-26.4477505196712,24.9798947491,-4.27993994259104));
#39615=CARTESIAN_POINT('Ctrl Pts',(-26.5426305894621,24.7688601285093,-4.2647945691676));
#39616=CARTESIAN_POINT('Ctrl Pts',(-26.6616210091264,24.4040282169322,-4.23894265356162));
#39617=CARTESIAN_POINT('Ctrl Pts',(-26.6986553303595,24.2553107148667,-4.2285091352454));
#39618=CARTESIAN_POINT('Ctrl Pts',(-26.732555814328,24.0611372282712,-4.21534249098413));
#39619=CARTESIAN_POINT('Ctrl Pts',(-26.739240739655,24.0175980659007,-4.21241999084546));
#39620=CARTESIAN_POINT('Ctrl Pts',(-26.7540046924746,23.9062701927076,-4.20504359664744));
#39621=CARTESIAN_POINT('Ctrl Pts',(-26.7608269565842,23.8383322897388,-4.20063247990639));
#39622=CARTESIAN_POINT('Ctrl Pts',(-26.7662361143637,23.7592686292224,-4.19564183160193));
#39623=CARTESIAN_POINT('Ctrl Pts',(-26.7669296135479,23.7483098274811,-4.19495327324181));
#39624=CARTESIAN_POINT('Ctrl Pts',(-26.7677585821542,23.7340547532595,-4.19406192926262));
#39625=CARTESIAN_POINT('Ctrl Pts',(-26.7679450101344,23.7307616888622,-4.19385631984731));
#39626=CARTESIAN_POINT('Ctrl Pts',(-26.7682391236181,23.7254211937342,-4.19352336750498));
#39627=CARTESIAN_POINT('Ctrl Pts',(-26.7683499108297,23.7233739469517,-4.19339584961283));
#39628=CARTESIAN_POINT('Ctrl Pts',(-26.7685589002173,23.7194424861783,-4.19315119596635));
#39629=CARTESIAN_POINT('Ctrl Pts',(-26.7686574010694,23.717558297197,-4.19303404388137));
#39630=CARTESIAN_POINT('Ctrl Pts',(-26.7688801581254,23.7132242533887,-4.19276479795247));
#39631=CARTESIAN_POINT('Ctrl Pts',(-26.7690032722777,23.710774336405,-4.19261276894541));
#39632=CARTESIAN_POINT('Ctrl Pts',(-26.769385334552,23.7029942664259,-4.19213050651392));
#39633=CARTESIAN_POINT('Ctrl Pts',(-26.769633842675,23.6976635741591,-4.1918008601863));
#39634=CARTESIAN_POINT('Ctrl Pts',(-26.7716439370443,23.6521135582221,-4.18899061305948));
#39635=CARTESIAN_POINT('Ctrl Pts',(-26.7726651043539,23.6118628633773,-4.18655082835764));
#39636=CARTESIAN_POINT('Ctrl Pts',(-26.7729762871449,23.5648887716828,-4.18374330021972));
#39637=CARTESIAN_POINT('Ctrl Pts',(-26.7729997826694,23.5581759949475,-4.18334304171166));
#39638=CARTESIAN_POINT('Ctrl Pts',(-26.7730352005879,23.4638902064783,-4.17773382955586));
#39639=CARTESIAN_POINT('Ctrl Pts',(-26.7694985965574,23.3763453175803,-4.17267913867162));
#39640=CARTESIAN_POINT('Ctrl Pts',(-26.7330214650367,22.9277716066589,-4.14708892265759));
#39641=CARTESIAN_POINT('Ctrl Pts',(-26.6429182559604,22.574072100136,-4.12760012635231));
#39642=CARTESIAN_POINT('Ctrl Pts',(-26.4875583442566,22.2240660387918,-4.10444298478342));
#39643=CARTESIAN_POINT('Ctrl Pts',(-26.4790811376852,22.2054480785495,-4.10319994645464));
#39644=CARTESIAN_POINT('Ctrl Pts',(-26.4677783248097,22.1812382796036,-4.1015684013831));
#39645=CARTESIAN_POINT('Ctrl Pts',(-26.4651127280699,22.1755719103747,-4.10118544138217));
#39646=CARTESIAN_POINT('Ctrl Pts',(-26.4609813743745,22.1668557642111,-4.10059466511295));
#39647=CARTESIAN_POINT('Ctrl Pts',(-26.4595272904305,22.1638004445542,-4.10038725469932));
#39648=CARTESIAN_POINT('Ctrl Pts',(-26.4566270511556,22.1577311168639,-4.09997459461927));
#39649=CARTESIAN_POINT('Ctrl Pts',(-26.4551810124597,22.1547170575343,-4.09976934920925));
#39650=CARTESIAN_POINT('Ctrl Pts',(-26.4519722757289,22.1480555052654,-4.0993150213823));
#39651=CARTESIAN_POINT('Ctrl Pts',(-26.4502073867011,22.1444090793393,-4.09906586277491));
#39652=CARTESIAN_POINT('Ctrl Pts',(-26.4451168713067,22.1339419727684,-4.09834930169176));
#39653=CARTESIAN_POINT('Ctrl Pts',(-26.4417740408908,22.1271297315254,-4.09788129837131));
#39654=CARTESIAN_POINT('Ctrl Pts',(-26.41961775824,22.082378534663,-4.09479592768817));
#39655=CARTESIAN_POINT('Ctrl Pts',(-26.400082885085,22.0448032448244,-4.09215331248392));
#39656=CARTESIAN_POINT('Ctrl Pts',(-26.3403090337582,21.9351631643943,-4.08428305681629));
#39657=CARTESIAN_POINT('Ctrl Pts',(-26.2980382631075,21.8642511767335,-4.07898433132942));
#39658=CARTESIAN_POINT('Ctrl Pts',(-26.0907800909265,21.5450945605374,-4.05415252330508));
#39659=CARTESIAN_POINT('Ctrl Pts',(-25.894612645465,21.3189139456743,-4.03352932944031));
#39660=CARTESIAN_POINT('Ctrl Pts',(-25.6023429951045,21.0636569134999,-4.00786187434773));
#39661=CARTESIAN_POINT('Ctrl Pts',(-25.5320287122559,21.0072622161041,-4.00201267575824));
#39662=CARTESIAN_POINT('Ctrl Pts',(-25.4542682034371,20.9500827228878,-3.99596179866068));
#39663=CARTESIAN_POINT('Ctrl Pts',(-25.4490887651295,20.9462979097507,-3.99556068299996));
#39664=CARTESIAN_POINT('Ctrl Pts',(-25.4418928488262,20.9410724662449,-3.99500609747454));
#39665=CARTESIAN_POINT('Ctrl Pts',(-25.4398860028496,20.9396186913926,-3.99485172025148));
#39666=CARTESIAN_POINT('Ctrl Pts',(-25.4364346787909,20.9371245900839,-3.9945867257879));
#39667=CARTESIAN_POINT('Ctrl Pts',(-25.4349910159461,20.9360831459684,-3.99447603052115));
#39668=CARTESIAN_POINT('Ctrl Pts',(-25.432008033712,20.933935007505,-3.99424761604955));
#39669=CARTESIAN_POINT('Ctrl Pts',(-25.4304686035824,20.9328284774414,-3.99412990876358));
#39670=CARTESIAN_POINT('Ctrl Pts',(-25.426853597266,20.9302348747746,-3.99385389814171));
#39671=CARTESIAN_POINT('Ctrl Pts',(-25.4247772231676,20.92874890533,-3.99369567191777));
#39672=CARTESIAN_POINT('Ctrl Pts',(-25.4180346489997,20.9239356488915,-3.99318285648074));
#39673=CARTESIAN_POINT('Ctrl Pts',(-25.4133613052385,20.9206183164923,-3.99282895481266));
#39674=CARTESIAN_POINT('Ctrl Pts',(-25.2855445550673,20.8304004894742,-3.98319078770374));
#39675=CARTESIAN_POINT('Ctrl Pts',(-25.1564449971852,20.7522187494271,-3.9744921697016));
#39676=CARTESIAN_POINT('Ctrl Pts',(-24.7151557101342,20.5256285403925,-3.94643849774397));
#39677=CARTESIAN_POINT('Ctrl Pts',(-24.384668685978,20.4183050047682,-3.9277304383771));
#39678=CARTESIAN_POINT('Ctrl Pts',(-24.0229605670322,20.3622917079563,-3.90559981502139));
#39679=CARTESIAN_POINT('Ctrl Pts',(-24.0024496603143,20.3593177429465,-3.90434059196153));
#39680=CARTESIAN_POINT('Ctrl Pts',(-23.9756744755184,20.3556988307987,-3.90269075525043));
#39681=CARTESIAN_POINT('Ctrl Pts',(-23.9694346691237,20.3548740700774,-3.90230584429812));
#39682=CARTESIAN_POINT('Ctrl Pts',(-23.9598303164005,20.3536332090516,-3.90171271876441));
#39683=CARTESIAN_POINT('Ctrl Pts',(-23.95646743828,20.3532041265015,-3.90150491527495));
#39684=CARTESIAN_POINT('Ctrl Pts',(-23.949819283781,20.352366521674,-3.90109385227066));
#39685=CARTESIAN_POINT('Ctrl Pts',(-23.9465340421302,20.3519577537207,-3.90089060079857));
#39686=CARTESIAN_POINT('Ctrl Pts',(-23.9393316361947,20.3510728581137,-3.90044473387189));
#39687=CARTESIAN_POINT('Ctrl Pts',(-23.9354142197083,20.3505988617989,-3.9002020513401));
#39688=CARTESIAN_POINT('Ctrl Pts',(-23.9243390675044,20.3492794336721,-3.89951545329457));
#39689=CARTESIAN_POINT('Ctrl Pts',(-23.9171793855118,20.34845082123,-3.89907100688035));
#39690=CARTESIAN_POINT('Ctrl Pts',(-23.9011557486698,20.3466508073824,-3.89807498506227));
#39691=CARTESIAN_POINT('Ctrl Pts',(-23.8922904462955,20.3456921658871,-3.89752300951158));
#39692=CARTESIAN_POINT('Ctrl Pts',(-23.7133926031724,20.3270980263835,-3.88636561931689));
#39693=CARTESIAN_POINT('Ctrl Pts',(-23.5422566705809,20.3229845631223,-3.87532777304698));
#39694=CARTESIAN_POINT('Ctrl Pts',(-23.0502725751672,20.3502957859667,-3.84259033391797));
#39695=CARTESIAN_POINT('Ctrl Pts',(-22.7334270007086,20.416167060159,-3.82011092006373));
#39696=CARTESIAN_POINT('Ctrl Pts',(-22.4165915220138,20.5334352597712,-3.79873398439484));
#39697=CARTESIAN_POINT('Ctrl Pts',(-22.4016224429598,20.5391028041678,-3.7977272553634));
#39698=CARTESIAN_POINT('Ctrl Pts',(-22.3833668039644,20.5461706412306,-3.79650400697162));
#39699=CARTESIAN_POINT('Ctrl Pts',(-22.3800398875701,20.5474650477008,-3.79628126576141));
#39700=CARTESIAN_POINT('Ctrl Pts',(-22.3745542427759,20.5496098540189,-3.79591430726386));
#39701=CARTESIAN_POINT('Ctrl Pts',(-22.3723942817149,20.5504570572196,-3.79576989812885));
#39702=CARTESIAN_POINT('Ctrl Pts',(-22.3684982173198,20.5519900703166,-3.79550956473558));
#39703=CARTESIAN_POINT('Ctrl Pts',(-22.3667617993054,20.5526750542541,-3.79539359087805));
#39704=CARTESIAN_POINT('Ctrl Pts',(-22.3630255631325,20.5541526810375,-3.7951441650494));
#39705=CARTESIAN_POINT('Ctrl Pts',(-22.3610259487391,20.5549458154391,-3.79501074376876));
#39706=CARTESIAN_POINT('Ctrl Pts',(-22.3555428367392,20.5571270133287,-3.79464507987255));
#39707=CARTESIAN_POINT('Ctrl Pts',(-22.352060951305,20.5585191610653,-3.79441308495365));
#39708=CARTESIAN_POINT('Ctrl Pts',(-22.3338662600028,20.5658307274141,-3.79320184258342));
#39709=CARTESIAN_POINT('Ctrl Pts',(-22.319194530257,20.5718527450191,-3.79222873446555));
#39710=CARTESIAN_POINT('Ctrl Pts',(-22.1722495732096,20.633437715581,-3.78251312207513));
#39711=CARTESIAN_POINT('Ctrl Pts',(-22.0437635840609,20.6976742278776,-3.77426476093259));
#39712=CARTESIAN_POINT('Ctrl Pts',(-21.6267526061687,20.9422241995619,-3.74696759628441));
#39713=CARTESIAN_POINT('Ctrl Pts',(-21.3626139583364,21.1594589909255,-3.72850667866777));
#39714=CARTESIAN_POINT('Ctrl Pts',(-21.1235919601499,21.4294358612213,-3.70670416997352));
#39715=CARTESIAN_POINT('Ctrl Pts',(-21.1100386460553,21.4450444563176,-3.70544818310043));
#39716=CARTESIAN_POINT('Ctrl Pts',(-21.0925600250056,21.4655691887136,-3.70380200237777));
#39717=CARTESIAN_POINT('Ctrl Pts',(-21.0884974217569,21.4703681897785,-3.70341747986854));
#39718=CARTESIAN_POINT('Ctrl Pts',(-21.0822668792514,21.4777719247301,-3.70282482207802));
#39719=CARTESIAN_POINT('Ctrl Pts',(-21.0800889449977,21.4803682591501,-3.70261709684376));
#39720=CARTESIAN_POINT('Ctrl Pts',(-21.0757914412457,21.485507793277,-3.70220610707547));
#39721=CARTESIAN_POINT('Ctrl Pts',(-21.0736716871212,21.4880508337198,-3.70200285044926));
#39722=CARTESIAN_POINT('Ctrl Pts',(-21.0690330794048,21.4936331760292,-3.70155689138208));
#39723=CARTESIAN_POINT('Ctrl Pts',(-21.066515886424,21.4966738452943,-3.7013141217089));
#39724=CARTESIAN_POINT('Ctrl Pts',(-21.0594289312271,21.5052666971676,-3.70062845468206));
#39725=CARTESIAN_POINT('Ctrl Pts',(-21.0548721775985,21.5108295350825,-3.70018503007203));
#39726=CARTESIAN_POINT('Ctrl Pts',(-21.0447124636344,21.5233174366792,-3.69919060342048));
#39727=CARTESIAN_POINT('Ctrl Pts',(-21.0391195368424,21.5302505535615,-3.69863920011983));
#39728=CARTESIAN_POINT('Ctrl Pts',(-20.9272495564966,21.6701096904999,-3.68752938780932));
#39729=CARTESIAN_POINT('Ctrl Pts',(-20.8316561569087,21.8112014951871,-3.67654249566736));
#39730=CARTESIAN_POINT('Ctrl Pts',(-20.5883397552585,22.2397855599911,-3.64380605066535));
#39731=CARTESIAN_POINT('Ctrl Pts',(-20.4720815894401,22.5427275385657,-3.62126333245579));
#39732=CARTESIAN_POINT('Ctrl Pts',(-20.3993304900804,22.8734496917229,-3.59983763236267));
#39733=CARTESIAN_POINT('Ctrl Pts',(-20.3960204589618,22.8890476822934,-3.59883475592369));
#39734=CARTESIAN_POINT('Ctrl Pts',(-20.3921121155843,22.9081626753874,-3.59761561700886));
#39735=CARTESIAN_POINT('Ctrl Pts',(-20.3914037730136,22.9116565784314,-3.59739318103359));
#39736=CARTESIAN_POINT('Ctrl Pts',(-20.3902442949107,22.9174248441887,-3.59702662196992));
#39737=CARTESIAN_POINT('Ctrl Pts',(-20.3897898163113,22.9196985186562,-3.59688230775134));
#39738=CARTESIAN_POINT('Ctrl Pts',(-20.3889739068327,22.9238034097067,-3.5966220761213));
#39739=CARTESIAN_POINT('Ctrl Pts',(-20.3886116140037,22.9256344451101,-3.59650610929064));
#39740=CARTESIAN_POINT('Ctrl Pts',(-20.3878349876222,22.9295775187021,-3.59625662125887));
#39741=CARTESIAN_POINT('Ctrl Pts',(-20.3874211801551,22.9316896516296,-3.59612313088746));
#39742=CARTESIAN_POINT('Ctrl Pts',(-20.3862912455956,22.9374877792008,-3.59575708575434));
#39743=CARTESIAN_POINT('Ctrl Pts',(-20.3855794412158,22.9411746281617,-3.5955247795546));
#39744=CARTESIAN_POINT('Ctrl Pts',(-20.3818827416378,22.9605034197248,-3.59430920405122));
#39745=CARTESIAN_POINT('Ctrl Pts',(-20.3790072989027,22.9761664408064,-3.5933321265163));
#39746=CARTESIAN_POINT('Ctrl Pts',(-20.3446353925671,23.1715392765327,-3.58123631951792));
#39747=CARTESIAN_POINT('Ctrl Pts',(-20.3283338742798,23.3536172110083,-3.57092003762428));
#39748=CARTESIAN_POINT('Ctrl Pts',(-20.3264155662258,23.7910437246479,-3.546414951305));
#39749=CARTESIAN_POINT('Ctrl Pts',(-20.3555465001149,24.0451730283263,-3.53233784307375));
#39750=CARTESIAN_POINT('Ctrl Pts',(-20.4152279643893,24.2970820721114,-3.51701193552946));
#39751=CARTESIAN_POINT('Ctrl Pts',(-20.4161525807257,24.3009528028979,-3.51677612997515));
#39752=CARTESIAN_POINT('Ctrl Pts',(-20.4194497917377,24.3146436819744,-3.51594095560996));
#39753=CARTESIAN_POINT('Ctrl Pts',(-20.4218613740993,24.3244543070197,-3.51534043769612));
#39754=CARTESIAN_POINT('Ctrl Pts',(-20.4256159599233,24.3394244260853,-3.51442088676505));
#39755=CARTESIAN_POINT('Ctrl Pts',(-20.4269257166613,24.3445922515533,-3.51410286240769));
#39756=CARTESIAN_POINT('Ctrl Pts',(-20.4287787146652,24.3518280700543,-3.51365674188052));
#39757=CARTESIAN_POINT('Ctrl Pts',(-20.429311204817,24.3538988271829,-3.51352897472617));
#39758=CARTESIAN_POINT('Ctrl Pts',(-20.4315377732023,24.362521958183,-3.51299652069353));
#39759=CARTESIAN_POINT('Ctrl Pts',(-20.433250420032,24.369069483708,-3.51259126493477));
#39760=CARTESIAN_POINT('Ctrl Pts',(-20.436820080891,24.382542958108,-3.5117553123687));
#39761=CARTESIAN_POINT('Ctrl Pts',(-20.4386796100524,24.3894681962741,-3.51132453939361));
#39762=CARTESIAN_POINT('Ctrl Pts',(-20.4482211809661,24.4245351119534,-3.50913758772434));
#39763=CARTESIAN_POINT('Ctrl Pts',(-20.456261761692,24.452577063105,-3.50737019098676));
#39764=CARTESIAN_POINT('Ctrl Pts',(-20.4665415219874,24.4866741701049,-3.50519719693621));
#39765=CARTESIAN_POINT('Ctrl Pts',(-20.4684198248075,24.4928374043096,-3.50480345615348));
#39766=CARTESIAN_POINT('Ctrl Pts',(-20.4715469573693,24.5029891251625,-3.50415330900261));
#39767=CARTESIAN_POINT('Ctrl Pts',(-20.4727850920539,24.5069809088238,-3.50389725422928));
#39768=CARTESIAN_POINT('Ctrl Pts',(-20.4750300715203,24.5141693409945,-3.50343540763567));
#39769=CARTESIAN_POINT('Ctrl Pts',(-20.4760341461147,24.5173668540156,-3.50322970722053));
#39770=CARTESIAN_POINT('Ctrl Pts',(-20.4781629643227,24.5241093407096,-3.50279539247604));
#39771=CARTESIAN_POINT('Ctrl Pts',(-20.4792888596168,24.5276539430982,-3.50256674045236));
#39772=CARTESIAN_POINT('Ctrl Pts',(-20.4821900936578,24.5367332581924,-3.50198021557083));
#39773=CARTESIAN_POINT('Ctrl Pts',(-20.4839742691022,24.5422651138169,-3.50162205160463));
#39774=CARTESIAN_POINT('Ctrl Pts',(-20.4879801556456,24.5545713484214,-3.5008234680341));
#39775=CARTESIAN_POINT('Ctrl Pts',(-20.4902093957214,24.5613432276342,-3.50038280070358));
#39776=CARTESIAN_POINT('Ctrl Pts',(-20.4968278079865,24.5812259446431,-3.49908534428002));
#39777=CARTESIAN_POINT('Ctrl Pts',(-20.5012788601949,24.5943158738596,-3.49822650917489));
#39778=CARTESIAN_POINT('Ctrl Pts',(-20.516897735719,24.6392970723253,-3.49525902731987));
#39779=CARTESIAN_POINT('Ctrl Pts',(-20.5284825005611,24.6710402317541,-3.49313660688906));
#39780=CARTESIAN_POINT('Ctrl Pts',(-20.5827162007208,24.8126879077974,-3.48353531152221));
#39781=CARTESIAN_POINT('Ctrl Pts',(-20.6308727650596,24.9203734392677,-3.47587559667729));
#39782=CARTESIAN_POINT('Ctrl Pts',(-20.8286714649276,25.3046525981251,-3.44723972970496));
#39783=CARTESIAN_POINT('Ctrl Pts',(-21.0126263332655,25.561560694453,-3.42531753112927));
#39784=CARTESIAN_POINT('Ctrl Pts',(-21.2339531419561,25.790987839493,-3.40490572696321));
#39785=CARTESIAN_POINT('Ctrl Pts',(-21.2370663655839,25.7942015827925,-3.40461965517891));
#39786=CARTESIAN_POINT('Ctrl Pts',(-21.2438387697025,25.8011635827133,-3.40399962691574));
#39787=CARTESIAN_POINT('Ctrl Pts',(-21.2475004250445,25.8049094318148,-3.40366583269406));
#39788=CARTESIAN_POINT('Ctrl Pts',(-21.2572754629531,25.814860577897,-3.4027786076108));
#39789=CARTESIAN_POINT('Ctrl Pts',(-21.2634049492402,25.8210500962439,-3.4022262684138));
#39790=CARTESIAN_POINT('Ctrl Pts',(-21.270674587486,25.8283316456735,-3.4015759771239));
#39791=CARTESIAN_POINT('Ctrl Pts',(-21.2717904645627,25.8294477102464,-3.40147629106471));
#39792=CARTESIAN_POINT('Ctrl Pts',(-21.2823384999536,25.8399820301659,-3.40053524515658));
#39793=CARTESIAN_POINT('Ctrl Pts',(-21.2918283779793,25.849342696996,-3.39969807371846));
#39794=CARTESIAN_POINT('Ctrl Pts',(-21.3039984438396,25.8611989908464,-3.39863679023316));
#39795=CARTESIAN_POINT('Ctrl Pts',(-21.3066249994441,25.863749119355,-3.39840846800066));
#39796=CARTESIAN_POINT('Ctrl Pts',(-21.3108030025703,25.8677917446093,-3.39804643896065));
#39797=CARTESIAN_POINT('Ctrl Pts',(-21.3123516000185,25.8692871620874,-3.39791250285376));
#39798=CARTESIAN_POINT('Ctrl Pts',(-21.3152456604843,25.8720762398894,-3.3976626710656));
#39799=CARTESIAN_POINT('Ctrl Pts',(-21.3165907400274,25.8733702744633,-3.39754674606989));
#39800=CARTESIAN_POINT('Ctrl Pts',(-21.3196088053085,25.8762687615408,-3.39728706029532));
#39801=CARTESIAN_POINT('Ctrl Pts',(-21.3212823946222,25.8778725745053,-3.39714334997494));
#39802=CARTESIAN_POINT('Ctrl Pts',(-21.3262279120883,25.882601675097,-3.39671953549956));
#39803=CARTESIAN_POINT('Ctrl Pts',(-21.3295047106563,25.885721895932,-3.3964398268374));
#39804=CARTESIAN_POINT('Ctrl Pts',(-21.3549189839264,25.9098199307345,-3.39427886627923));
#39805=CARTESIAN_POINT('Ctrl Pts',(-21.3773476225397,25.9304903595793,-3.39242103874771));
#39806=CARTESIAN_POINT('Ctrl Pts',(-21.4557033991246,26.0006729390814,-3.38608421457666));
#39807=CARTESIAN_POINT('Ctrl Pts',(-21.5130595459458,26.0485605045044,-3.38170916989849));
#39808=CARTESIAN_POINT('Ctrl Pts',(-21.6789319459723,26.1775350233767,-3.36961023167016));
#39809=CARTESIAN_POINT('Ctrl Pts',(-21.7909699180333,26.2538395365431,-3.36206294142898));
#39810=CARTESIAN_POINT('Ctrl Pts',(-21.96242393445,26.3554256659843,-3.35092737772661));
#39811=CARTESIAN_POINT('Ctrl Pts',(-22.0183009156529,26.3863262187569,-3.34735930310875));
#39812=CARTESIAN_POINT('Ctrl Pts',(-22.0750361667496,26.4155368525077,-3.34376876818698));
#39813=CARTESIAN_POINT('Origin',(-23.5502525316942,23.5502525316942,-77.3107734492734));
#39814=CARTESIAN_POINT('',(-22.0750359636318,26.4155367479307,-1.84841977781535));
#39815=CARTESIAN_POINT('',(-22.0750363389647,26.4155369411741,-2.09574775951102));
#39816=CARTESIAN_POINT('',(-22.0750360153461,26.4155367745563,-77.3107734492734));
#39817=CARTESIAN_POINT('Ctrl Pts',(-22.0750359636318,26.4155367479307,-1.84841977781534));
#39818=CARTESIAN_POINT('Ctrl Pts',(-22.0147494710243,26.3844977214282,-1.85229280629613));
#39819=CARTESIAN_POINT('Ctrl Pts',(-21.9554363723595,26.3515528266262,-1.85611401846149));
#39820=CARTESIAN_POINT('Ctrl Pts',(-21.7891319966047,26.2521808848818,-1.86697516491533));
#39821=CARTESIAN_POINT('Ctrl Pts',(-21.6849533142671,26.1813399344116,-1.87396327472071));
#39822=CARTESIAN_POINT('Ctrl Pts',(-21.431080192038,25.9860336499376,-1.89203649308758));
#39823=CARTESIAN_POINT('Ctrl Pts',(-21.288044137719,25.8537969097466,-1.9032641130977));
#39824=CARTESIAN_POINT('Ctrl Pts',(-21.1511518557094,25.7021196591162,-1.91570441433683));
#39825=CARTESIAN_POINT('Ctrl Pts',(-21.1445322562156,25.6947166000034,-1.91631051088979));
#39826=CARTESIAN_POINT('Ctrl Pts',(-21.134949831241,25.683899844989,-1.91719456263574));
#39827=CARTESIAN_POINT('Ctrl Pts',(-21.1319597578092,25.6805102747366,-1.91747137504461));
#39828=CARTESIAN_POINT('Ctrl Pts',(-21.1267362191044,25.674563660496,-1.91795663752941));
#39829=CARTESIAN_POINT('Ctrl Pts',(-21.1244996402559,25.6720093506712,-1.91816495721126));
#39830=CARTESIAN_POINT('Ctrl Pts',(-21.120173268853,25.6670525878746,-1.91856898180749));
#39831=CARTESIAN_POINT('Ctrl Pts',(-21.1180829913787,25.6646505615306,-1.91876466621032));
#39832=CARTESIAN_POINT('Ctrl Pts',(-21.1131147864482,25.6589242715424,-1.91923092094093));
#39833=CARTESIAN_POINT('Ctrl Pts',(-21.1102401007902,25.6555972142755,-1.91950162538642));
#39834=CARTESIAN_POINT('Ctrl Pts',(-21.100053254489,25.6437584384739,-1.92046419478591));
#39835=CARTESIAN_POINT('Ctrl Pts',(-21.0927788153043,25.6352144996606,-1.92115761539434));
#39836=CARTESIAN_POINT('Ctrl Pts',(-20.98748006118,25.5102228551447,-1.93128419140052));
#39837=CARTESIAN_POINT('Ctrl Pts',(-20.8977963235191,25.3870296474176,-1.94105711520603));
#39838=CARTESIAN_POINT('Ctrl Pts',(-20.6899568360752,25.0543974038987,-1.96694913272589));
#39839=CARTESIAN_POINT('Ctrl Pts',(-20.5859015751572,24.8372451535808,-1.98343988181253));
#39840=CARTESIAN_POINT('Ctrl Pts',(-20.4925954809956,24.5694431279525,-2.00236342484556));
#39841=CARTESIAN_POINT('Ctrl Pts',(-20.4790948647286,24.5280086250873,-2.00525107353723));
#39842=CARTESIAN_POINT('Ctrl Pts',(-20.451792775599,24.4380628359811,-2.01141648684609));
#39843=CARTESIAN_POINT('Ctrl Pts',(-20.4382807966536,24.3894739220751,-2.01468348435445));
#39844=CARTESIAN_POINT('Ctrl Pts',(-20.4220161424861,24.3251765732929,-2.01890624316303));
#39845=CARTESIAN_POINT('Ctrl Pts',(-20.4182323544617,24.3097390754593,-2.01991256150456));
#39846=CARTESIAN_POINT('Ctrl Pts',(-20.4130052999681,24.2877095713463,-2.02133724389597));
#39847=CARTESIAN_POINT('Ctrl Pts',(-20.4114683575524,24.2811403400346,-2.02176065372164));
#39848=CARTESIAN_POINT('Ctrl Pts',(-20.4091436878043,24.2710616113708,-2.02240801681774));
#39849=CARTESIAN_POINT('Ctrl Pts',(-20.4083411991506,24.26755558985,-2.02263279473431));
#39850=CARTESIAN_POINT('Ctrl Pts',(-20.4070301156251,24.2617831359981,-2.02300218520011));
#39851=CARTESIAN_POINT('Ctrl Pts',(-20.4065181013511,24.2595174957921,-2.02314699237782));
#39852=CARTESIAN_POINT('Ctrl Pts',(-20.4055579057269,24.2552472063919,-2.02341959239409));
#39853=CARTESIAN_POINT('Ctrl Pts',(-20.405109191057,24.2532426801614,-2.02354741591625));
#39854=CARTESIAN_POINT('Ctrl Pts',(-20.4042649330627,24.2494541698359,-2.02378873653539));
#39855=CARTESIAN_POINT('Ctrl Pts',(-20.4038689918767,24.2476702845046,-2.02390225621014));
#39856=CARTESIAN_POINT('Ctrl Pts',(-20.4030655257328,24.2440357132869,-2.0241333218128));
#39857=CARTESIAN_POINT('Ctrl Pts',(-20.4026581174377,24.2421850117388,-2.02425086064171));
#39858=CARTESIAN_POINT('Ctrl Pts',(-20.4014934609144,24.2368721038966,-2.02458794877002));
#39859=CARTESIAN_POINT('Ctrl Pts',(-20.4007402880225,24.2334089925422,-2.02480726241004));
#39860=CARTESIAN_POINT('Ctrl Pts',(-20.3974867472199,24.21832937255,-2.02576047410109));
#39861=CARTESIAN_POINT('Ctrl Pts',(-20.395044882047,24.2067001343429,-2.02649104213994));
#39862=CARTESIAN_POINT('Ctrl Pts',(-20.3918912978707,24.1912571523086,-2.02745550344502));
#39863=CARTESIAN_POINT('Ctrl Pts',(-20.3911221039985,24.1874554413979,-2.02769247516465));
#39864=CARTESIAN_POINT('Ctrl Pts',(-20.3235565072747,23.8503854879869,-2.04866330793441));
#39865=CARTESIAN_POINT('Ctrl Pts',(-20.3098811304207,23.5085855880593,-2.06666543409453));
#39866=CARTESIAN_POINT('Ctrl Pts',(-20.3613807979946,23.0741031048338,-2.09159407772048));
#39867=CARTESIAN_POINT('Ctrl Pts',(-20.3772414981934,22.9778716755029,-2.09723151325793));
#39868=CARTESIAN_POINT('Ctrl Pts',(-20.4105758942607,22.8204793688928,-2.10675239907097));
#39869=CARTESIAN_POINT('Ctrl Pts',(-20.4255411068997,22.7588512948536,-2.11055760018341));
#39870=CARTESIAN_POINT('Ctrl Pts',(-20.4445337607476,22.689613862309,-2.11493398504481));
#39871=CARTESIAN_POINT('Ctrl Pts',(-20.4467856102481,22.6815287154898,-2.11544660748937));
#39872=CARTESIAN_POINT('Ctrl Pts',(-20.4502169249906,22.6693923826968,-2.11621848540238));
#39873=CARTESIAN_POINT('Ctrl Pts',(-20.4513728178548,22.6653345220406,-2.1164769714898));
#39874=CARTESIAN_POINT('Ctrl Pts',(-20.4533750193501,22.6583576539857,-2.11692209784983));
#39875=CARTESIAN_POINT('Ctrl Pts',(-20.4542174965111,22.6554375451413,-2.11710861271907));
#39876=CARTESIAN_POINT('Ctrl Pts',(-20.4559615280675,22.6494245090397,-2.11749311752306));
#39877=CARTESIAN_POINT('Ctrl Pts',(-20.4568635919321,22.646331733861,-2.11769112396119));
#39878=CARTESIAN_POINT('Ctrl Pts',(-20.459047229259,22.6388865643088,-2.11816835715027));
#39879=CARTESIAN_POINT('Ctrl Pts',(-20.4603333569777,22.634535522076,-2.11844773281111));
#39880=CARTESIAN_POINT('Ctrl Pts',(-20.4643113746801,22.6211814695238,-2.11930665046801));
#39881=CARTESIAN_POINT('Ctrl Pts',(-20.4670334380588,22.6121875655245,-2.11988718087699));
#39882=CARTESIAN_POINT('Ctrl Pts',(-20.499430669127,22.5068091344996,-2.12671343279464));
#39883=CARTESIAN_POINT('Ctrl Pts',(-20.533571918748,22.4118665830744,-2.13310607655239));
#39884=CARTESIAN_POINT('Ctrl Pts',(-20.6829344098437,22.050680663392,-2.1584179011844));
#39885=CARTESIAN_POINT('Ctrl Pts',(-20.8294304198555,21.7988796130966,-2.17837549436561));
#39886=CARTESIAN_POINT('Ctrl Pts',(-21.0346001927308,21.5354210626815,-2.20067816442014));
#39887=CARTESIAN_POINT('Ctrl Pts',(-21.0623363300044,21.5012708833047,-2.20359658498709));
#39888=CARTESIAN_POINT('Ctrl Pts',(-21.1346569859304,21.4158604723975,-2.21094631091168));
#39889=CARTESIAN_POINT('Ctrl Pts',(-21.1801818715847,21.3654189108885,-2.21533534267922));
#39890=CARTESIAN_POINT('Ctrl Pts',(-21.2323016317085,21.3112183946938,-2.22007052553823));
#39891=CARTESIAN_POINT('Ctrl Pts',(-21.2373501413318,21.3060037093855,-2.22052630197605));
#39892=CARTESIAN_POINT('Ctrl Pts',(-21.2450631522409,21.2980904887591,-2.2212181790071));
#39893=CARTESIAN_POINT('Ctrl Pts',(-21.2477148300794,21.2953795694694,-2.22145524646465));
#39894=CARTESIAN_POINT('Ctrl Pts',(-21.2520559274166,21.2909571296145,-2.22184204634748));
#39895=CARTESIAN_POINT('Ctrl Pts',(-21.2537424791541,21.2892428182157,-2.22199200033308));
#39896=CARTESIAN_POINT('Ctrl Pts',(-21.2569957405921,21.2859434053518,-2.22228063237449));
#39897=CARTESIAN_POINT('Ctrl Pts',(-21.2585621779397,21.2843580389708,-2.22241933167617));
#39898=CARTESIAN_POINT('Ctrl Pts',(-21.2614162990792,21.2814754153301,-2.22267154358612));
#39899=CARTESIAN_POINT('Ctrl Pts',(-21.2627034375136,21.2801776330993,-2.22278509850839));
#39900=CARTESIAN_POINT('Ctrl Pts',(-21.2653228527705,21.277541047108,-2.22301581170385));
#39901=CARTESIAN_POINT('Ctrl Pts',(-21.2666551973533,21.2762023245896,-2.22313296356487));
#39902=CARTESIAN_POINT('Ctrl Pts',(-21.2704689601419,21.2723770369018,-2.22346773970981));
#39903=CARTESIAN_POINT('Ctrl Pts',(-21.272953277985,21.2698933467783,-2.22368513346133));
#39904=CARTESIAN_POINT('Ctrl Pts',(-21.2836705569123,21.2592137568224,-2.22462005712921));
#39905=CARTESIAN_POINT('Ctrl Pts',(-21.2919438729133,21.2510582102517,-2.22533441216096));
#39906=CARTESIAN_POINT('Ctrl Pts',(-21.4337118112802,21.1128118098934,-2.23745419650848));
#39907=CARTESIAN_POINT('Ctrl Pts',(-21.578223806049,20.9944773510963,-2.24799918387846));
#39908=CARTESIAN_POINT('Ctrl Pts',(-21.8704444700303,20.7948207535242,-2.26782783903187));
#39909=CARTESIAN_POINT('Ctrl Pts',(-22.0158580193115,20.711275460077,-2.2771040514605));
#39910=CARTESIAN_POINT('Ctrl Pts',(-22.2608480388759,20.5948631976761,-2.29260916806692));
#39911=CARTESIAN_POINT('Ctrl Pts',(-22.3566830066463,20.554876284831,-2.29864281321902));
#39912=CARTESIAN_POINT('Ctrl Pts',(-22.4992202695564,20.5033306253284,-2.30768024299628));
#39913=CARTESIAN_POINT('Ctrl Pts',(-22.5445206006651,20.488079311462,-2.31056103798599));
#39914=CARTESIAN_POINT('Ctrl Pts',(-22.5976242230304,20.4715063077072,-2.31395350221476));
#39915=CARTESIAN_POINT('Ctrl Pts',(-22.6051153311819,20.4691983814596,-2.31443241370109));
#39916=CARTESIAN_POINT('Ctrl Pts',(-22.6165413100471,20.4657237571691,-2.31516344317922));
#39917=CARTESIAN_POINT('Ctrl Pts',(-22.6204701500044,20.4645371966779,-2.3154149092318));
#39918=CARTESIAN_POINT('Ctrl Pts',(-22.6276057801377,20.4623970092866,-2.31587181281953));
#39919=CARTESIAN_POINT('Ctrl Pts',(-22.630811813879,20.4614408634777,-2.31607716748746));
#39920=CARTESIAN_POINT('Ctrl Pts',(-22.6377095436108,20.4593954219885,-2.31651913388153));
#39921=CARTESIAN_POINT('Ctrl Pts',(-22.6414017107691,20.4583077451857,-2.31675579823457));
#39922=CARTESIAN_POINT('Ctrl Pts',(-22.6513284088281,20.4554027524761,-2.31739234113963));
#39923=CARTESIAN_POINT('Ctrl Pts',(-22.6575664746471,20.4535976692398,-2.31779261888205));
#39924=CARTESIAN_POINT('Ctrl Pts',(-22.6860906322902,20.4454371045188,-2.31962417754935));
#39925=CARTESIAN_POINT('Ctrl Pts',(-22.7084389705096,20.4393033986791,-2.32106267069402));
#39926=CARTESIAN_POINT('Ctrl Pts',(-22.7441404480199,20.4299176642449,-2.32336668488871));
#39927=CARTESIAN_POINT('Ctrl Pts',(-22.7574518789417,20.4265090255754,-2.32422706871126));
#39928=CARTESIAN_POINT('Ctrl Pts',(-22.7746922098383,20.4222116163076,-2.32534316680685));
#39929=CARTESIAN_POINT('Ctrl Pts',(-22.7786016904003,20.4212448998623,-2.32559637461803));
#39930=CARTESIAN_POINT('Ctrl Pts',(-22.8719335985539,20.3983518153624,-2.33164408398727));
#39931=CARTESIAN_POINT('Ctrl Pts',(-22.9622451083185,20.380262111649,-2.3375597882004));
#39932=CARTESIAN_POINT('Ctrl Pts',(-23.2535104046101,20.3347955608054,-2.35684083989997));
#39933=CARTESIAN_POINT('Ctrl Pts',(-23.4563070529969,20.3225013816433,-2.37060292748258));
#39934=CARTESIAN_POINT('Ctrl Pts',(-23.8323688226921,20.3351852175872,-2.39603546999539));
#39935=CARTESIAN_POINT('Ctrl Pts',(-24.0051180095531,20.3550434753913,-2.40766911660469));
#39936=CARTESIAN_POINT('Ctrl Pts',(-24.182300219831,20.3900813168716,-2.41903825277547));
#39937=CARTESIAN_POINT('Ctrl Pts',(-24.1891505841266,20.3914591437376,-2.41947690417789));
#39938=CARTESIAN_POINT('Ctrl Pts',(-24.1996107846104,20.3935984436739,-2.42014525489775));
#39939=CARTESIAN_POINT('Ctrl Pts',(-24.2032238314059,20.3943438425652,-2.42037584445405));
#39940=CARTESIAN_POINT('Ctrl Pts',(-24.2091476753078,20.3955765848886,-2.42075346881158));
#39941=CARTESIAN_POINT('Ctrl Pts',(-24.2114592183555,20.3960602646897,-2.42090071078288));
#39942=CARTESIAN_POINT('Ctrl Pts',(-24.2159194783303,20.3969986722074,-2.42118460620677));
#39943=CARTESIAN_POINT('Ctrl Pts',(-24.2180682651042,20.3974530562293,-2.42132127928002));
#39944=CARTESIAN_POINT('Ctrl Pts',(-24.2220033838607,20.3982893828075,-2.42157139146125));
#39945=CARTESIAN_POINT('Ctrl Pts',(-24.2237898478976,20.3986706458708,-2.42168486909836));
#39946=CARTESIAN_POINT('Ctrl Pts',(-24.2274425893842,20.3994534532963,-2.4219167547322));
#39947=CARTESIAN_POINT('Ctrl Pts',(-24.2293088271958,20.3998551354513,-2.42203515415357));
#39948=CARTESIAN_POINT('Ctrl Pts',(-24.2347065620429,20.401021943173,-2.42237738979209));
#39949=CARTESIAN_POINT('Ctrl Pts',(-24.2382371450628,20.4017913533707,-2.42260097875961));
#39950=CARTESIAN_POINT('Ctrl Pts',(-24.2539674364746,20.4052471351741,-2.42359602486919));
#39951=CARTESIAN_POINT('Ctrl Pts',(-24.2661529730728,20.4079985347341,-2.42436378219493));
#39952=CARTESIAN_POINT('Ctrl Pts',(-24.2809707024383,20.4114349345807,-2.42529399432965));
#39953=CARTESIAN_POINT('Ctrl Pts',(-24.2836182002076,20.4120524505353,-2.42546006426578));
#39954=CARTESIAN_POINT('Ctrl Pts',(-24.6186463471903,20.4906432530917,-2.44645907733329));
#39955=CARTESIAN_POINT('Ctrl Pts',(-24.9365912207545,20.6209460095237,-2.46453112471705));
#39956=CARTESIAN_POINT('Ctrl Pts',(-25.3094915595013,20.8483526109719,-2.48942519613442));
#39957=CARTESIAN_POINT('Ctrl Pts',(-25.3885475015473,20.9015066867624,-2.49493227117917));
#39958=CARTESIAN_POINT('Ctrl Pts',(-25.5170412457105,20.996426968454,-2.5043811475226));
#39959=CARTESIAN_POINT('Ctrl Pts',(-25.5677856147155,21.0363228954142,-2.50825295102506));
#39960=CARTESIAN_POINT('Ctrl Pts',(-25.6237599961517,21.0831174822532,-2.51270010475568));
#39961=CARTESIAN_POINT('Ctrl Pts',(-25.6302031545065,21.0885470330856,-2.51321472964418));
#39962=CARTESIAN_POINT('Ctrl Pts',(-25.6398458023128,21.0967376274924,-2.51398902745751));
#39963=CARTESIAN_POINT('Ctrl Pts',(-25.6430613093975,21.0994798287585,-2.51424792373933));
#39964=CARTESIAN_POINT('Ctrl Pts',(-25.6485807468954,21.104205617486,-2.51469351916355));
#39965=CARTESIAN_POINT('Ctrl Pts',(-25.6508872869714,21.1061861598389,-2.5148800921569));
#39966=CARTESIAN_POINT('Ctrl Pts',(-25.6556303148301,21.1102704999486,-2.51526449607886));
#39967=CARTESIAN_POINT('Ctrl Pts',(-25.658066459394,21.1123746899984,-2.51546234318443));
#39968=CARTESIAN_POINT('Ctrl Pts',(-25.6639214649186,21.1174472162411,-2.51593883032677));
#39969=CARTESIAN_POINT('Ctrl Pts',(-25.6673372245128,21.1204191083331,-2.51621761825719));
#39970=CARTESIAN_POINT('Ctrl Pts',(-25.6777936842519,21.1295555700323,-2.51707355044855));
#39971=CARTESIAN_POINT('Ctrl Pts',(-25.6848137586981,21.1357435751503,-2.51765167376828));
#39972=CARTESIAN_POINT('Ctrl Pts',(-25.7659289690192,21.2078746646212,-2.52437255498367));
#39973=CARTESIAN_POINT('Ctrl Pts',(-25.8369612907692,21.2771674689656,-2.53065737607574));
#39974=CARTESIAN_POINT('Ctrl Pts',(-26.1037372978666,21.5625874765751,-2.55594096521853));
#39975=CARTESIAN_POINT('Ctrl Pts',(-26.2729617071288,21.8015669520083,-2.5760008784623));
#39976=CARTESIAN_POINT('Ctrl Pts',(-26.4280808220543,22.0989911635446,-2.59840672463539));
#39977=CARTESIAN_POINT('Ctrl Pts',(-26.4476353990424,22.1384352522685,-2.60132742165609));
#39978=CARTESIAN_POINT('Ctrl Pts',(-26.4953716663972,22.2398977403806,-2.60869198233823));
#39979=CARTESIAN_POINT('Ctrl Pts',(-26.5224085178665,22.3024357249117,-2.6130932923653));
#39980=CARTESIAN_POINT('Ctrl Pts',(-26.5514753314337,22.3759870090907,-2.61807366895531));
#39981=CARTESIAN_POINT('Ctrl Pts',(-26.5554536057793,22.3862060017614,-2.6187613018492));
#39982=CARTESIAN_POINT('Ctrl Pts',(-26.5605599486011,22.3995233343494,-2.61965161921877));
#39983=CARTESIAN_POINT('Ctrl Pts',(-26.5617354694051,22.4026032185262,-2.61985711955954));
#39984=CARTESIAN_POINT('Ctrl Pts',(-26.5636342496168,22.4076010598323,-2.62018993402235));
#39985=CARTESIAN_POINT('Ctrl Pts',(-26.5643604047698,22.4095179027913,-2.62031742285892));
#39986=CARTESIAN_POINT('Ctrl Pts',(-26.5657514575433,22.4132004877643,-2.6205620478331));
#39987=CARTESIAN_POINT('Ctrl Pts',(-26.5664166313607,22.4149661157185,-2.6206792002514));
#39988=CARTESIAN_POINT('Ctrl Pts',(-26.5679432483283,22.419029157905,-2.62094848388521));
#39989=CARTESIAN_POINT('Ctrl Pts',(-26.5688036207641,22.4213269781532,-2.62110055018736));
#39990=CARTESIAN_POINT('Ctrl Pts',(-26.5714610080558,22.4284488920648,-2.6215711780463));
#39991=CARTESIAN_POINT('Ctrl Pts',(-26.5732491002714,22.4332763409159,-2.62188920425452));
#39992=CARTESIAN_POINT('Ctrl Pts',(-26.5878355494606,22.4729480756384,-2.62449485293776));
#39993=CARTESIAN_POINT('Ctrl Pts',(-26.6000432457672,22.5080086201089,-2.62674781694578));
#39994=CARTESIAN_POINT('Ctrl Pts',(-26.7182993195313,22.8675277574703,-2.64942044096342));
#39995=CARTESIAN_POINT('Ctrl Pts',(-26.7727812658795,23.2067101508008,-2.66747027613089));
#39996=CARTESIAN_POINT('Ctrl Pts',(-26.7730375089227,23.6033534261096,-2.69026412956738));
#39997=CARTESIAN_POINT('Ctrl Pts',(-26.7716558194149,23.6585259170155,-2.69346620726019));
#39998=CARTESIAN_POINT('Ctrl Pts',(-26.768433196616,23.7220114806858,-2.69720044260653));
#39999=CARTESIAN_POINT('Ctrl Pts',(-26.7679752288546,23.7303874007087,-2.69769410891723));
#40000=CARTESIAN_POINT('Ctrl Pts',(-26.7633890991607,23.8086576948525,-2.70231687388276));
#40001=CARTESIAN_POINT('Ctrl Pts',(-26.7570171911784,23.8783974946396,-2.70650808168359));
#40002=CARTESIAN_POINT('Ctrl Pts',(-26.7472251429439,23.9571570088781,-2.71134202467801));
#40003=CARTESIAN_POINT('Ctrl Pts',(-26.7460301619426,23.9664381462107,-2.71191324542094));
#40004=CARTESIAN_POINT('Ctrl Pts',(-26.744209844536,23.9801058530803,-2.71275681846786));
#40005=CARTESIAN_POINT('Ctrl Pts',(-26.743615849142,23.9844966066453,-2.71302817796419));
#40006=CARTESIAN_POINT('Ctrl Pts',(-26.7425509698524,23.9922477331081,-2.71350786046206));
#40007=CARTESIAN_POINT('Ctrl Pts',(-26.7420838289907,23.995608620458,-2.71371606454762));
#40008=CARTESIAN_POINT('Ctrl Pts',(-26.741106514098,24.0025594779948,-2.71414710919673));
#40009=CARTESIAN_POINT('Ctrl Pts',(-26.7405955875958,24.0061493360075,-2.71436997334935));
#40010=CARTESIAN_POINT('Ctrl Pts',(-26.7392709848073,24.0153449470342,-2.71494148511913));
#40011=CARTESIAN_POINT('Ctrl Pts',(-26.7384485880384,24.0209494137298,-2.71529040901676));
#40012=CARTESIAN_POINT('Ctrl Pts',(-26.7350247798169,24.043861287917,-2.7167193516256));
#40013=CARTESIAN_POINT('Ctrl Pts',(-26.7322972153144,24.0611492811752,-2.71780336947734));
#40014=CARTESIAN_POINT('Ctrl Pts',(-26.7134677529929,24.1744899833767,-2.72494938209993));
#40015=CARTESIAN_POINT('Ctrl Pts',(-26.6931611394368,24.269783717082,-2.73114481910676));
#40016=CARTESIAN_POINT('Ctrl Pts',(-26.6316782401347,24.5053879987416,-2.74695124763146));
#40017=CARTESIAN_POINT('Ctrl Pts',(-26.5852141185865,24.6440844777718,-2.75670789053095));
#40018=CARTESIAN_POINT('Ctrl Pts',(-26.4358911206073,25.006096566825,-2.783146228409));
#40019=CARTESIAN_POINT('Ctrl Pts',(-26.3166401197718,25.2216330422663,-2.7999791957612));
#40020=CARTESIAN_POINT('Ctrl Pts',(-26.1658445077554,25.4330686060118,-2.81638506190913));
#40021=CARTESIAN_POINT('Ctrl Pts',(-26.1575529433625,25.4445340144293,-2.81727412190962));
#40022=CARTESIAN_POINT('Ctrl Pts',(-26.1469721090427,25.4589638812027,-2.81839193755103));
#40023=CARTESIAN_POINT('Ctrl Pts',(-26.1447529877117,25.4619792284769,-2.81862546053773));
#40024=CARTESIAN_POINT('Ctrl Pts',(-26.1412381292602,25.4667378338647,-2.81899388240071));
#40025=CARTESIAN_POINT('Ctrl Pts',(-26.1399458845009,25.4684836488243,-2.81912902438785));
#40026=CARTESIAN_POINT('Ctrl Pts',(-26.1375408885669,25.4717259242929,-2.81937996135543));
#40027=CARTESIAN_POINT('Ctrl Pts',(-26.1364286104118,25.4732227160637,-2.81949578806962));
#40028=CARTESIAN_POINT('Ctrl Pts',(-26.1339459130093,25.4765576296768,-2.81975381531637));
#40029=CARTESIAN_POINT('Ctrl Pts',(-26.1325748343275,25.4783952506251,-2.81989596829689));
#40030=CARTESIAN_POINT('Ctrl Pts',(-26.1285642346391,25.4837586016909,-2.82031078905726));
#40031=CARTESIAN_POINT('Ctrl Pts',(-26.1259194322612,25.4872804040098,-2.82058308632838));
#40032=CARTESIAN_POINT('Ctrl Pts',(-26.1067641607551,25.5126788446631,-2.8225462594122));
#40033=CARTESIAN_POINT('Ctrl Pts',(-26.0899817859081,25.5343503567916,-2.82421828213052));
#40034=CARTESIAN_POINT('Ctrl Pts',(-26.0364471629167,25.6016885181801,-2.82941318009864));
#40035=CARTESIAN_POINT('Ctrl Pts',(-25.9987225735468,25.6465704262292,-2.83287505864796));
#40036=CARTESIAN_POINT('Ctrl Pts',(-25.9048215732454,25.7522912125675,-2.84109725080491));
#40037=CARTESIAN_POINT('Ctrl Pts',(-25.8474837298069,25.8120438590498,-2.84580200400116));
#40038=CARTESIAN_POINT('Ctrl Pts',(-25.6274551384789,26.0243292548041,-2.8630193164219));
#40039=CARTESIAN_POINT('Ctrl Pts',(-25.4513809742409,26.1620594148432,-2.875260611496));
#40040=CARTESIAN_POINT('Ctrl Pts',(-25.1616018363719,26.3437907261885,-2.89500747817153));
#40041=CARTESIAN_POINT('Ctrl Pts',(-25.0572836209951,26.4014197397457,-2.90203705754552));
#40042=CARTESIAN_POINT('Ctrl Pts',(-24.9404305573871,26.4577662561175,-2.90993069201774));
#40043=CARTESIAN_POINT('Ctrl Pts',(-24.9308141331345,26.4623446767304,-2.91058039641108));
#40044=CARTESIAN_POINT('Ctrl Pts',(-24.9172841026905,26.4687043015373,-2.91149470924142));
#40045=CARTESIAN_POINT('Ctrl Pts',(-24.9133892842406,26.4705255056757,-2.91175793048819));
#40046=CARTESIAN_POINT('Ctrl Pts',(-24.9066266716694,26.4736712039743,-2.91221500839286));
#40047=CARTESIAN_POINT('Ctrl Pts',(-24.9037605459633,26.474999289318,-2.91240874056708));
#40048=CARTESIAN_POINT('Ctrl Pts',(-24.8978574182098,26.4777241039893,-2.91280778544201));
#40049=CARTESIAN_POINT('Ctrl Pts',(-24.8948201877655,26.4791203257183,-2.9130131153483));
#40050=CARTESIAN_POINT('Ctrl Pts',(-24.8877125887241,26.4823743193437,-2.91349366106644));
#40051=CARTESIAN_POINT('Ctrl Pts',(-24.8836405202389,26.4842283416561,-2.91376900578269));
#40052=CARTESIAN_POINT('Ctrl Pts',(-24.8750399258782,26.4881226093017,-2.91435063225017));
#40053=CARTESIAN_POINT('Ctrl Pts',(-24.8705105216409,26.4901608758828,-2.91465698136322));
#40054=CARTESIAN_POINT('Ctrl Pts',(-24.8583533418804,26.4955979389077,-2.91547936233691));
#40055=CARTESIAN_POINT('Ctrl Pts',(-24.8507170760723,26.498977555176,-2.91599605195103));
#40056=CARTESIAN_POINT('Ctrl Pts',(-24.6670811050053,26.5793980725762,-2.92842480170463));
#40057=CARTESIAN_POINT('Ctrl Pts',(-24.4845890141806,26.6405631951537,-2.9408885364234));
#40058=CARTESIAN_POINT('Ctrl Pts',(-24.0042889811236,26.7550918308312,-2.97386858086621));
#40059=CARTESIAN_POINT('Ctrl Pts',(-23.702445504781,26.783515040905,-2.99485014069555));
#40060=CARTESIAN_POINT('Ctrl Pts',(-23.3849598488456,26.7688011934813,-3.01496249244831));
#40061=CARTESIAN_POINT('Ctrl Pts',(-23.3688705336006,26.7679345787353,-3.01597598091149));
#40062=CARTESIAN_POINT('Ctrl Pts',(-23.3492164031156,26.76672806275,-3.01720643545685));
#40063=CARTESIAN_POINT('Ctrl Pts',(-23.3456451526113,26.7665028620643,-3.01742970866661));
#40064=CARTESIAN_POINT('Ctrl Pts',(-23.3397563797149,26.7661216720056,-3.01779735897987));
#40065=CARTESIAN_POINT('Ctrl Pts',(-23.3374386506163,26.765969125192,-3.01794192919325));
#40066=CARTESIAN_POINT('Ctrl Pts',(-23.3332585126869,26.7656894604644,-3.01820242948673));
#40067=CARTESIAN_POINT('Ctrl Pts',(-23.3313960539708,26.7655632304294,-3.01831840948071));
#40068=CARTESIAN_POINT('Ctrl Pts',(-23.3273896882546,26.7652881977364,-3.0185677110303));
#40069=CARTESIAN_POINT('Ctrl Pts',(-23.3252458260677,26.7651388692491,-3.01870100214614));
#40070=CARTESIAN_POINT('Ctrl Pts',(-23.3193707299076,26.764723739964,-3.01906596911516));
#40071=CARTESIAN_POINT('Ctrl Pts',(-23.3156397918937,26.7644535860547,-3.0192973988299));
#40072=CARTESIAN_POINT('Ctrl Pts',(-23.2962094457437,26.7630126401227,-3.02050092957759));
#40073=CARTESIAN_POINT('Ctrl Pts',(-23.280517945837,26.7617332930951,-3.02146698387324));
#40074=CARTESIAN_POINT('Ctrl Pts',(-23.1255891668766,26.7479582051925,-3.03095257659426));
#40075=CARTESIAN_POINT('Ctrl Pts',(-22.9872758710674,26.7265283740593,-3.0390029099222));
#40076=CARTESIAN_POINT('Ctrl Pts',(-22.5809545265929,26.636185394098,-3.06253153655113));
#40077=CARTESIAN_POINT('Ctrl Pts',(-22.320271996219,26.5417986630288,-3.07757178124686));
#40078=CARTESIAN_POINT('Ctrl Pts',(-22.0750359182355,26.4155367245581,-3.0937462422167));
#40079=CARTESIAN_POINT('',(-26.7730011298473,23.5526187726184,-2.93758573339873));
#40080=CARTESIAN_POINT('Ctrl Pts',(-22.0750361667496,26.4155368525077,-3.34376876818698));
#40081=CARTESIAN_POINT('Ctrl Pts',(-22.1688943408046,26.4638605435787,-3.3378288799319));
#40082=CARTESIAN_POINT('Ctrl Pts',(-22.2651012992214,26.5075592847051,-3.33182564982117));
#40083=CARTESIAN_POINT('Ctrl Pts',(-22.4572788829981,26.5836897363742,-3.31980480788063));
#40084=CARTESIAN_POINT('Ctrl Pts',(-22.5529345878195,26.6164694787834,-3.31380812174433));
#40085=CARTESIAN_POINT('Ctrl Pts',(-22.6589933387836,26.6473258303721,-3.30708520147718));
#40086=CARTESIAN_POINT('Ctrl Pts',(-22.6680327218927,26.6499128631793,-3.30651165196124));
#40087=CARTESIAN_POINT('Ctrl Pts',(-22.6814520928204,26.6536899741265,-3.3056593254318));
#40088=CARTESIAN_POINT('Ctrl Pts',(-22.6858235386818,26.6549104319104,-3.30538153864854));
#40089=CARTESIAN_POINT('Ctrl Pts',(-22.6933028319005,26.6569815441514,-3.30490602365386));
#40090=CARTESIAN_POINT('Ctrl Pts',(-22.6964094127031,26.6578367820177,-3.30470844488574));
#40091=CARTESIAN_POINT('Ctrl Pts',(-22.7026418186639,26.6595425046275,-3.30431192085007));
#40092=CARTESIAN_POINT('Ctrl Pts',(-22.7057676533225,26.6603929379636,-3.30411297421242));
#40093=CARTESIAN_POINT('Ctrl Pts',(-22.7120507913711,26.6620921956407,-3.30371293168302));
#40094=CARTESIAN_POINT('Ctrl Pts',(-22.7152081143956,26.6629409312299,-3.30351183318725));
#40095=CARTESIAN_POINT('Ctrl Pts',(-22.7252528880012,26.6656247333638,-3.30287181502195));
#40096=CARTESIAN_POINT('Ctrl Pts',(-22.7321451019116,26.667441746204,-3.30243230962323));
#40097=CARTESIAN_POINT('Ctrl Pts',(-22.7723843216199,26.6779074734242,-3.29986417558199));
#40098=CARTESIAN_POINT('Ctrl Pts',(-22.8058612053786,26.6860436266896,-3.29771901156181));
#40099=CARTESIAN_POINT('Ctrl Pts',(-22.9032067568754,26.708055662676,-3.29145374148205));
#40100=CARTESIAN_POINT('Ctrl Pts',(-22.9673721276543,26.7205266983352,-3.28728963235783));
#40101=CARTESIAN_POINT('Ctrl Pts',(-23.145642830397,26.7495801041324,-3.27562146042933));
#40102=CARTESIAN_POINT('Ctrl Pts',(-23.2603194225701,26.7620028817506,-3.26800160186077));
#40103=CARTESIAN_POINT('Ctrl Pts',(-23.6616752211399,26.7838101247049,-3.24105942298021));
#40104=CARTESIAN_POINT('Ctrl Pts',(-23.948742506596,26.7610978109878,-3.2211910774191));
#40105=CARTESIAN_POINT('Ctrl Pts',(-24.2415967046084,26.6980019208678,-3.20223802942282));
#40106=CARTESIAN_POINT('Ctrl Pts',(-24.254153687607,26.6952177394838,-3.20142820987855));
#40107=CARTESIAN_POINT('Ctrl Pts',(-24.2718131105254,26.6911911592768,-3.20029366698206));
#40108=CARTESIAN_POINT('Ctrl Pts',(-24.2769294928991,26.6900113960249,-3.19996547557595));
#40109=CARTESIAN_POINT('Ctrl Pts',(-24.2845064884599,26.688244738203,-3.19948023378188));
#40110=CARTESIAN_POINT('Ctrl Pts',(-24.2869692982333,26.6876674496073,-3.19932263507599));
#40111=CARTESIAN_POINT('Ctrl Pts',(-24.2911775537826,26.6866757959197,-3.19905355648742));
#40112=CARTESIAN_POINT('Ctrl Pts',(-24.2929233327316,26.6862628732036,-3.19894199314404));
#40113=CARTESIAN_POINT('Ctrl Pts',(-24.2963223017574,26.6854559300348,-3.19872490705267));
#40114=CARTESIAN_POINT('Ctrl Pts',(-24.297975520261,26.6850620607003,-3.19861937614539));
#40115=CARTESIAN_POINT('Ctrl Pts',(-24.3019628353981,26.6841087732498,-3.19836498819468));
#40116=CARTESIAN_POINT('Ctrl Pts',(-24.3042966249379,26.6835480538187,-3.19821620703586));
#40117=CARTESIAN_POINT('Ctrl Pts',(-24.3114207402016,26.6818279837734,-3.19776237740747));
#40118=CARTESIAN_POINT('Ctrl Pts',(-24.3162090632844,26.6806602441475,-3.19745781377138));
#40119=CARTESIAN_POINT('Ctrl Pts',(-24.3646782151912,26.668722089187,-3.19437948094654));
#40120=CARTESIAN_POINT('Ctrl Pts',(-24.4081343625763,26.6570484447148,-3.19165715215846));
#40121=CARTESIAN_POINT('Ctrl Pts',(-24.5309914502857,26.621270617972,-3.18403105931695));
#40122=CARTESIAN_POINT('Ctrl Pts',(-24.6097291853234,26.5950041171786,-3.17922784467167));
#40123=CARTESIAN_POINT('Ctrl Pts',(-24.7945841085958,26.5252963517135,-3.16796451724521));
#40124=CARTESIAN_POINT('Ctrl Pts',(-24.8995688105568,26.4791762694943,-3.16157672544629));
#40125=CARTESIAN_POINT('Ctrl Pts',(-25.1168980558848,26.3695319707076,-3.14797462472122));
#40126=CARTESIAN_POINT('Ctrl Pts',(-25.2283319684792,26.3046602445977,-3.14076668697122));
#40127=CARTESIAN_POINT('Ctrl Pts',(-25.3828567008539,26.201837770413,-3.13012641416181));
#40128=CARTESIAN_POINT('Ctrl Pts',(-25.4292920356733,26.169136337539,-3.12683950056204));
#40129=CARTESIAN_POINT('Ctrl Pts',(-25.4905088274792,26.1235587300766,-3.12236638170538));
#40130=CARTESIAN_POINT('Ctrl Pts',(-25.506073385003,26.1117489793259,-3.1212165402572));
#40131=CARTESIAN_POINT('Ctrl Pts',(-25.5256327317084,26.0966259393591,-3.11975504412438));
#40132=CARTESIAN_POINT('Ctrl Pts',(-25.5297284094047,26.0934433847364,-3.11944808324342));
#40133=CARTESIAN_POINT('Ctrl Pts',(-25.5370532965627,26.087723152366,-3.11889742250627));
#40134=CARTESIAN_POINT('Ctrl Pts',(-25.540285377806,26.0851891583637,-3.11865385687884));
#40135=CARTESIAN_POINT('Ctrl Pts',(-25.5461453740895,26.0805767302907,-3.1182111778378));
#40136=CARTESIAN_POINT('Ctrl Pts',(-25.5487749119699,26.0785003604769,-3.11801214051021));
#40137=CARTESIAN_POINT('Ctrl Pts',(-25.5927391309593,26.0436733179728,-3.11467770188953));
#40138=CARTESIAN_POINT('Ctrl Pts',(-25.6332650533486,26.0099185791214,-3.1115051547378));
#40139=CARTESIAN_POINT('Ctrl Pts',(-25.6795060496545,25.9694410528153,-3.10776003941509));
#40140=CARTESIAN_POINT('Ctrl Pts',(-25.6860458240265,25.9636693325271,-3.10722737893163));
#40141=CARTESIAN_POINT('Ctrl Pts',(-25.69576412987,25.9550219418757,-3.10643131011997));
#40142=CARTESIAN_POINT('Ctrl Pts',(-25.6989605236228,25.9521663309785,-3.10616874527303));
#40143=CARTESIAN_POINT('Ctrl Pts',(-25.7046542744291,25.9470591571308,-3.10569972000538));
#40144=CARTESIAN_POINT('Ctrl Pts',(-25.7071538270086,25.9448100421689,-3.10549336312122));
#40145=CARTESIAN_POINT('Ctrl Pts',(-25.7119789536941,25.9404546745151,-3.10509412920712));
#40146=CARTESIAN_POINT('Ctrl Pts',(-25.7143049817363,25.9383489285077,-3.1049012737757));
#40147=CARTESIAN_POINT('Ctrl Pts',(-25.7193365550757,25.9337804729937,-3.10448323014683));
#40148=CARTESIAN_POINT('Ctrl Pts',(-25.7220409870032,25.9313165486108,-3.10425799043073));
#40149=CARTESIAN_POINT('Ctrl Pts',(-25.732673302807,25.9215965897878,-3.10337032069829));
#40150=CARTESIAN_POINT('Ctrl Pts',(-25.7405689961006,25.9143055863651,-3.10270639984789));
#40151=CARTESIAN_POINT('Ctrl Pts',(-25.8241802385079,25.8363192468397,-3.09562495571878));
#40152=CARTESIAN_POINT('Ctrl Pts',(-25.8964738505739,25.7620594381685,-3.08905269378531));
#40153=CARTESIAN_POINT('Ctrl Pts',(-26.0088972307174,25.6348545530367,-3.07804408436624));
#40154=CARTESIAN_POINT('Ctrl Pts',(-26.0511926417979,25.5839184422617,-3.07369619662488));
#40155=CARTESIAN_POINT('Ctrl Pts',(-26.252167109403,25.3261276206479,-3.05200658102386));
#40156=CARTESIAN_POINT('Ctrl Pts',(-26.3868968346137,25.1018682632967,-3.034004808293));
#40157=CARTESIAN_POINT('Ctrl Pts',(-26.4977419915785,24.8535371469987,-3.01611516702053));
#40158=CARTESIAN_POINT('Ctrl Pts',(-26.5022874803899,24.8432082820346,-3.01537472828653));
#40159=CARTESIAN_POINT('Ctrl Pts',(-26.5129664315766,24.8185922505983,-3.01361908472154));
#40160=CARTESIAN_POINT('Ctrl Pts',(-26.5190509981154,24.8042840216131,-3.01260576557898));
#40161=CARTESIAN_POINT('Ctrl Pts',(-26.52820989302,24.7823060099169,-3.01106078071371));
#40162=CARTESIAN_POINT('Ctrl Pts',(-26.5313585971773,24.7746676770487,-3.01052594657956));
#40163=CARTESIAN_POINT('Ctrl Pts',(-26.5354856424881,24.7645457255392,-3.00982008300289));
#40164=CARTESIAN_POINT('Ctrl Pts',(-26.53649029267,24.7620729480165,-3.00964786786068));
#40165=CARTESIAN_POINT('Ctrl Pts',(-26.5393134591315,24.7550993678874,-3.00916283999665));
#40166=CARTESIAN_POINT('Ctrl Pts',(-26.5411248880731,24.7505956805718,-3.00885035282926));
#40167=CARTESIAN_POINT('Ctrl Pts',(-26.5565328525252,24.7120360173548,-3.00618144869453));
#40168=CARTESIAN_POINT('Ctrl Pts',(-26.5695581193038,24.6777525490764,-3.00385214420757));
#40169=CARTESIAN_POINT('Ctrl Pts',(-26.5835826892461,24.6388514496286,-3.00126393461964));
#40170=CARTESIAN_POINT('Ctrl Pts',(-26.5851597624699,24.6344469561789,-3.00097167673504));
#40171=CARTESIAN_POINT('Ctrl Pts',(-26.5875268006212,24.6277905924981,-3.00053120100323));
#40172=CARTESIAN_POINT('Ctrl Pts',(-26.5883238558558,24.6255412773642,-3.0003825629187));
#40173=CARTESIAN_POINT('Ctrl Pts',(-26.5897031323159,24.6216351397674,-3.0001248017762));
#40174=CARTESIAN_POINT('Ctrl Pts',(-26.5902864975567,24.6199787270067,-3.00001561012724));
#40175=CARTESIAN_POINT('Ctrl Pts',(-26.5915023717629,24.6165173350041,-2.99978767040763));
#40176=CARTESIAN_POINT('Ctrl Pts',(-26.5921346273865,24.6147122709151,-2.9996689380268));
#40177=CARTESIAN_POINT('Ctrl Pts',(-26.5936387919884,24.6104056579456,-2.99938597940423));
#40178=CARTESIAN_POINT('Ctrl Pts',(-26.5945092266958,24.6079035873391,-2.99922184168739));
#40179=CARTESIAN_POINT('Ctrl Pts',(-26.5974298148769,24.5994748606458,-2.99866976533848));
#40180=CARTESIAN_POINT('Ctrl Pts',(-26.5994657707283,24.5935432462982,-2.99828266971334));
#40181=CARTESIAN_POINT('Ctrl Pts',(-26.6387551171952,24.4779790255854,-2.99076792548357));
#40182=CARTESIAN_POINT('Ctrl Pts',(-26.6700955626545,24.3664087776341,-2.98398354023975));
#40183=CARTESIAN_POINT('Ctrl Pts',(-26.7467938389344,24.0233349666376,-2.96385955048933));
#40184=CARTESIAN_POINT('Ctrl Pts',(-26.772828298777,23.7883472203177,-2.95102022401773));
#40185=CARTESIAN_POINT('Ctrl Pts',(-26.7730016601459,23.5526226717751,-2.93758688024679));
#40186=CARTESIAN_POINT('Ctrl Pts',(-26.7730016630494,23.5526187204738,-2.9375866550721));
#40187=CARTESIAN_POINT('Ctrl Pts',(-26.7731176149863,23.394692181726,-2.92858681874837));
#40188=CARTESIAN_POINT('Ctrl Pts',(-26.761625434773,23.2369872380094,-2.91936317422375));
#40189=CARTESIAN_POINT('Ctrl Pts',(-26.7376222489929,23.0739763744628,-2.90933099846862));
#40190=CARTESIAN_POINT('Ctrl Pts',(-26.7366004539343,23.0671877223873,-2.90891232305038));
#40191=CARTESIAN_POINT('Ctrl Pts',(-26.7348963751076,23.0561067614394,-2.90822746956691));
#40192=CARTESIAN_POINT('Ctrl Pts',(-26.7342270822599,23.0518124523366,-2.90796170356339));
#40193=CARTESIAN_POINT('Ctrl Pts',(-26.7330314354178,23.0442416374893,-2.90749252431895));
#40194=CARTESIAN_POINT('Ctrl Pts',(-26.7325087024492,23.0409645595176,-2.90728922628265));
#40195=CARTESIAN_POINT('Ctrl Pts',(-26.7314725822137,23.0345328715813,-2.90688981167449));
#40196=CARTESIAN_POINT('Ctrl Pts',(-26.7309595618014,23.0313782057139,-2.9066937069765));
#40197=CARTESIAN_POINT('Ctrl Pts',(-26.7299303083534,23.0251080066467,-2.90630353713853));
#40198=CARTESIAN_POINT('Ctrl Pts',(-26.7294141869646,23.0219924583332,-2.90610947574212));
#40199=CARTESIAN_POINT('Ctrl Pts',(-26.7281851937343,23.0146407211812,-2.90565109233367));
#40200=CARTESIAN_POINT('Ctrl Pts',(-26.7274684309178,23.0104051963617,-2.90538664662962));
#40201=CARTESIAN_POINT('Ctrl Pts',(-26.7249489607696,22.9956958652806,-2.90446701045664));
#40202=CARTESIAN_POINT('Ctrl Pts',(-26.7231029283755,22.9852296392551,-2.90381044068062));
#40203=CARTESIAN_POINT('Ctrl Pts',(-26.7001368033008,22.858683914779,-2.89584471742151));
#40204=CARTESIAN_POINT('Ctrl Pts',(-26.6727119668798,22.7438535494066,-2.88833377872145));
#40205=CARTESIAN_POINT('Ctrl Pts',(-26.6320720080184,22.6073284679076,-2.8790452970354));
#40206=CARTESIAN_POINT('Ctrl Pts',(-26.6248193302774,22.5839420066789,-2.87744142069908));
#40207=CARTESIAN_POINT('Ctrl Pts',(-26.6113050750688,22.5420580250215,-2.8745463312326));
#40208=CARTESIAN_POINT('Ctrl Pts',(-26.6051404628003,22.5235302985516,-2.87325763101354));
#40209=CARTESIAN_POINT('Ctrl Pts',(-26.5111682092076,22.2494376214018,-2.85407602357772));
#40210=CARTESIAN_POINT('Ctrl Pts',(-26.3917370846445,22.0058787904027,-2.8353921177336));
#40211=CARTESIAN_POINT('Ctrl Pts',(-26.205054281669,21.7218652959204,-2.81305161463466));
#40212=CARTESIAN_POINT('Ctrl Pts',(-26.1649020365322,21.6648926518335,-2.8085459738846));
#40213=CARTESIAN_POINT('Ctrl Pts',(-26.1162340942652,21.6003859170614,-2.80345654554986));
#40214=CARTESIAN_POINT('Ctrl Pts',(-26.1094913692146,21.5915443412106,-2.80275924387021));
#40215=CARTESIAN_POINT('Ctrl Pts',(-26.100679942838,21.5801133074973,-2.80185827764924));
#40216=CARTESIAN_POINT('Ctrl Pts',(-26.0986529256779,21.5774920357362,-2.80165171361203));
#40217=CARTESIAN_POINT('Ctrl Pts',(-26.0953630790357,21.5732512464698,-2.8013175951957));
#40218=CARTESIAN_POINT('Ctrl Pts',(-26.0941027446444,21.5716298101785,-2.80118986358982));
#40219=CARTESIAN_POINT('Ctrl Pts',(-26.0916822041781,21.5685218895532,-2.80094506447933));
#40220=CARTESIAN_POINT('Ctrl Pts',(-26.0905222468452,21.5670352232575,-2.80082798017312));
#40221=CARTESIAN_POINT('Ctrl Pts',(-26.0878547983203,21.5636226515896,-2.80055925096354));
#40222=CARTESIAN_POINT('Ctrl Pts',(-26.0863464155372,21.5616974390352,-2.80040767007954));
#40223=CARTESIAN_POINT('Ctrl Pts',(-26.0823237394377,21.5565751494944,-2.80000442558831));
#40224=CARTESIAN_POINT('Ctrl Pts',(-26.0798055725806,21.5533810988895,-2.7997530380818));
#40225=CARTESIAN_POINT('Ctrl Pts',(-26.0680043113549,21.5384704880372,-2.79857973190425));
#40226=CARTESIAN_POINT('Ctrl Pts',(-26.0586456231145,21.5268135940502,-2.79766313070836));
#40227=CARTESIAN_POINT('Ctrl Pts',(-25.8514212802897,21.2723486282651,-2.77765839200026));
#40228=CARTESIAN_POINT('Ctrl Pts',(-25.6192499451273,21.0595597780481,-2.76089459607937));
#40229=CARTESIAN_POINT('Ctrl Pts',(-25.2736455937428,20.8250149967025,-2.73726906027501));
#40230=CARTESIAN_POINT('Ctrl Pts',(-25.1845262947236,20.7706572387589,-2.73129002872255));
#40231=CARTESIAN_POINT('Ctrl Pts',(-25.0449716760142,20.6945711349221,-2.72196114427025));
#40232=CARTESIAN_POINT('Ctrl Pts',(-24.9963559554664,20.6696473989967,-2.71871778927306));
#40233=CARTESIAN_POINT('Ctrl Pts',(-24.9199963960683,20.6329205290624,-2.71361995107313));
#40234=CARTESIAN_POINT('Ctrl Pts',(-24.8926796055842,20.6202501897048,-2.71179561139613));
#40235=CARTESIAN_POINT('Ctrl Pts',(-24.8589483314576,20.6051753501253,-2.7095407486087));
#40236=CARTESIAN_POINT('Ctrl Pts',(-24.8526978620025,20.6024057815837,-2.70912283016058));
#40237=CARTESIAN_POINT('Ctrl Pts',(-24.8434716930708,20.5983527595356,-2.70850580483268));
#40238=CARTESIAN_POINT('Ctrl Pts',(-24.8405027655238,20.5970538593723,-2.70830722747293));
#40239=CARTESIAN_POINT('Ctrl Pts',(-24.8347453924039,20.5945453588049,-2.70792209917661));
#40240=CARTESIAN_POINT('Ctrl Pts',(-24.831957183881,20.593335220449,-2.70773556689757));
#40241=CARTESIAN_POINT('Ctrl Pts',(-24.8262102715081,20.5908506010729,-2.70735105212164));
#40242=CARTESIAN_POINT('Ctrl Pts',(-24.8232513609295,20.5895766086329,-2.70715305315777));
#40243=CARTESIAN_POINT('Ctrl Pts',(-24.8161213595973,20.5865193704512,-2.7066758805604));
#40244=CARTESIAN_POINT('Ctrl Pts',(-24.8119484124001,20.5847404941549,-2.70639655811985));
#40245=CARTESIAN_POINT('Ctrl Pts',(-24.7991234994463,20.579305360625,-2.70553794292718));
#40246=CARTESIAN_POINT('Ctrl Pts',(-24.7904593519459,20.5756781373682,-2.70495766275381));
#40247=CARTESIAN_POINT('Ctrl Pts',(-24.7584650396152,20.5624478839631,-2.70281393941075));
#40248=CARTESIAN_POINT('Ctrl Pts',(-24.7350386820786,20.5530812324948,-2.70124251294084));
#40249=CARTESIAN_POINT('Ctrl Pts',(-24.7058746754377,20.5418158184188,-2.69928357162428));
#40250=CARTESIAN_POINT('Ctrl Pts',(-24.7002379907897,20.5396566704131,-2.69890483582364));
#40251=CARTESIAN_POINT('Ctrl Pts',(-24.6881773104612,20.5350756059123,-2.69809419824144));
#40252=CARTESIAN_POINT('Ctrl Pts',(-24.6817515836279,20.5326583591457,-2.69766214363788));
#40253=CARTESIAN_POINT('Ctrl Pts',(-24.6738973158571,20.5297323346583,-2.69713383475595));
#40254=CARTESIAN_POINT('Ctrl Pts',(-24.6724760385455,20.5292039947892,-2.69703822601826));
#40255=CARTESIAN_POINT('Ctrl Pts',(-24.6647618547135,20.5263425503163,-2.69651925215158));
#40256=CARTESIAN_POINT('Ctrl Pts',(-24.658462081175,20.5240281183499,-2.69609527459557));
#40257=CARTESIAN_POINT('Ctrl Pts',(-24.643715625694,20.5186627376629,-2.69510245271877));
#40258=CARTESIAN_POINT('Ctrl Pts',(-24.6352633598522,20.5156273954722,-2.69453310441106));
#40259=CARTESIAN_POINT('Ctrl Pts',(-24.623045016367,20.5112971673876,-2.69370964352609));
#40260=CARTESIAN_POINT('Ctrl Pts',(-24.619288998891,20.5099738515407,-2.69345644681485));
#40261=CARTESIAN_POINT('Ctrl Pts',(-24.6105862289025,20.5069258226277,-2.69286964906068));
#40262=CARTESIAN_POINT('Ctrl Pts',(-24.6056377143004,20.5052062063694,-2.69253588639295));
#40263=CARTESIAN_POINT('Ctrl Pts',(-24.5805808568521,20.496567327377,-2.69084535846534));
#40264=CARTESIAN_POINT('Ctrl Pts',(-24.5604089340155,20.4898352735553,-2.68948271805058));
#40265=CARTESIAN_POINT('Ctrl Pts',(-24.4885166777385,20.4666305970646,-2.68462026064215));
#40266=CARTESIAN_POINT('Ctrl Pts',(-24.4364505785761,20.4512661898824,-2.68108751583845));
#40267=CARTESIAN_POINT('Ctrl Pts',(-24.2350708168662,20.3973300842698,-2.66738713078729));
#40268=CARTESIAN_POINT('Ctrl Pts',(-24.0834583137772,20.3681808258822,-2.65698375479044));
#40269=CARTESIAN_POINT('Ctrl Pts',(-23.9121277515839,20.3478314443187,-2.64530460500259));
#40270=CARTESIAN_POINT('Ctrl Pts',(-23.8938819539107,20.3458222676983,-2.64406200363223));
#40271=CARTESIAN_POINT('Ctrl Pts',(-23.8544243989858,20.3418181913229,-2.64137823439547));
#40272=CARTESIAN_POINT('Ctrl Pts',(-23.8332079350134,20.3398775243552,-2.63993729511466));
#40273=CARTESIAN_POINT('Ctrl Pts',(-23.7867649652777,20.3360933677338,-2.6367892804878));
#40274=CARTESIAN_POINT('Ctrl Pts',(-23.7615326892881,20.3343361802749,-2.63508297323784));
#40275=CARTESIAN_POINT('Ctrl Pts',(-23.7050297385417,20.3310691637154,-2.6312738230857));
#40276=CARTESIAN_POINT('Ctrl Pts',(-23.6737521200838,20.3297175669739,-2.6291733103008));
#40277=CARTESIAN_POINT('Ctrl Pts',(-23.5243564463918,20.3254414272693,-2.61919144697101));
#40278=CARTESIAN_POINT('Ctrl Pts',(-23.4061410277907,20.3285578987412,-2.61144270076675));
#40279=CARTESIAN_POINT('Ctrl Pts',(-23.2822617950769,20.3386585590301,-2.60365485502659));
#40280=CARTESIAN_POINT('Ctrl Pts',(-23.2761745462321,20.3391723178865,-2.60327302501202));
#40281=CARTESIAN_POINT('Ctrl Pts',(-23.2674777418531,20.3399312315853,-2.60272876328481));
#40282=CARTESIAN_POINT('Ctrl Pts',(-23.2648670156037,20.3401622620871,-2.602565541114));
#40283=CARTESIAN_POINT('Ctrl Pts',(-23.2603567323792,20.3405669354946,-2.60228384194877));
#40284=CARTESIAN_POINT('Ctrl Pts',(-23.25845704514,20.3407390802483,-2.60216527980001));
#40285=CARTESIAN_POINT('Ctrl Pts',(-23.2548022372927,20.3410735412371,-2.60193734641992));
#40286=CARTESIAN_POINT('Ctrl Pts',(-23.253047100458,20.341235610434,-2.60182796124331));
#40287=CARTESIAN_POINT('Ctrl Pts',(-23.2488909940216,20.3416228239484,-2.60156911542913));
#40288=CARTESIAN_POINT('Ctrl Pts',(-23.246490138292,20.341849223776,-2.60141972620068));
#40289=CARTESIAN_POINT('Ctrl Pts',(-23.2393343561126,20.3425321155418,-2.60097487528912));
#40290=CARTESIAN_POINT('Ctrl Pts',(-23.2345801611178,20.3429964871514,-2.60067985699347));
#40291=CARTESIAN_POINT('Ctrl Pts',(-23.1905864580744,20.3473923926164,-2.59795465659187));
#40292=CARTESIAN_POINT('Ctrl Pts',(-23.151419023337,20.352033506553,-2.59556375998345));
#40293=CARTESIAN_POINT('Ctrl Pts',(-23.1097927875592,20.3577426397597,-2.59305109765782));
#40294=CARTESIAN_POINT('Ctrl Pts',(-23.1072414710324,20.3580956751912,-2.5928972075835));
#40295=CARTESIAN_POINT('Ctrl Pts',(-23.1032624598652,20.3586511284116,-2.59265737550673));
#40296=CARTESIAN_POINT('Ctrl Pts',(-23.1018344788232,20.3588514457097,-2.59257133984019));
#40297=CARTESIAN_POINT('Ctrl Pts',(-23.0973154604185,20.3594884669021,-2.59229917862654));
#40298=CARTESIAN_POINT('Ctrl Pts',(-23.0942249137604,20.3599287049436,-2.59211320966619));
#40299=CARTESIAN_POINT('Ctrl Pts',(-22.8591971861004,20.3937561156087,-2.57798272765505));
#40300=CARTESIAN_POINT('Ctrl Pts',(-22.6315625206171,20.4523396940686,-2.56514371546771));
#40301=CARTESIAN_POINT('Ctrl Pts',(-22.2951364481622,20.5793138391578,-2.54498732163228));
#40302=CARTESIAN_POINT('Ctrl Pts',(-22.1806821305994,20.6303096017905,-2.5379095919147));
#40303=CARTESIAN_POINT('Ctrl Pts',(-22.0125182632425,20.7173025989869,-2.52691196314952));
#40304=CARTESIAN_POINT('Ctrl Pts',(-21.956441749928,20.7484676710725,-2.52313877769711));
#40305=CARTESIAN_POINT('Ctrl Pts',(-21.8764573241606,20.7960982995331,-2.5175780344988));
#40306=CARTESIAN_POINT('Ctrl Pts',(-21.8517811110839,20.8112471131967,-2.51583698431417));
#40307=CARTESIAN_POINT('Ctrl Pts',(-21.8168978247166,20.8333147501416,-2.51333756788259));
#40308=CARTESIAN_POINT('Ctrl Pts',(-21.8065206909193,20.839963117269,-2.51258914448544));
#40309=CARTESIAN_POINT('Ctrl Pts',(-21.7883134903224,20.8517758589677,-2.51126722198594));
#40310=CARTESIAN_POINT('Ctrl Pts',(-21.7804673143244,20.8569152300902,-2.51069465801427));
#40311=CARTESIAN_POINT('Ctrl Pts',(-21.7689735850154,20.8645157171566,-2.50985160759914));
#40312=CARTESIAN_POINT('Ctrl Pts',(-21.7653084082743,20.8669502008324,-2.50958212390627));
#40313=CARTESIAN_POINT('Ctrl Pts',(-21.7589897724524,20.8711658397017,-2.50911641906948));
#40314=CARTESIAN_POINT('Ctrl Pts',(-21.7563339493032,20.8729434543759,-2.50892033183641));
#40315=CARTESIAN_POINT('Ctrl Pts',(-21.7510593569301,20.8764852544787,-2.5085302063753));
#40316=CARTESIAN_POINT('Ctrl Pts',(-21.7484405273014,20.8782493442834,-2.50833617190397));
#40317=CARTESIAN_POINT('Ctrl Pts',(-21.7422664238528,20.8824215334286,-2.507877920129));
#40318=CARTESIAN_POINT('Ctrl Pts',(-21.7387133680811,20.8848328912111,-2.50761357930658));
#40319=CARTESIAN_POINT('Ctrl Pts',(-21.726391320236,20.8932315331307,-2.50669465175795));
#40320=CARTESIAN_POINT('Ctrl Pts',(-21.7176471786981,20.8992549984428,-2.50603868854075));
#40321=CARTESIAN_POINT('Ctrl Pts',(-21.6124850570262,20.9724656273743,-2.49810254509883));
#40322=CARTESIAN_POINT('Ctrl Pts',(-21.5197934187683,21.0448267924307,-2.4906222022246));
#40323=CARTESIAN_POINT('Ctrl Pts',(-21.2492041527251,21.2809609310822,-2.46720822712583));
#40324=CARTESIAN_POINT('Ctrl Pts',(-21.0856022918418,21.4598027245708,-2.45070297005883));
#40325=CARTESIAN_POINT('Ctrl Pts',(-20.855796525491,21.7759095638967,-2.42440150153338));
#40326=CARTESIAN_POINT('Ctrl Pts',(-20.7765246019652,21.9025778177085,-2.41450535977724));
#40327=CARTESIAN_POINT('Ctrl Pts',(-20.7034337725026,22.0396970354984,-2.40476921081609));
#40328=CARTESIAN_POINT('Ctrl Pts',(-20.7005727057971,22.0451014276156,-2.40438699748589));
#40329=CARTESIAN_POINT('Ctrl Pts',(-20.6965068436451,22.0528347592433,-2.40384228731023));
#40330=CARTESIAN_POINT('Ctrl Pts',(-20.6952895039893,22.0551570337856,-2.40367899822689));
#40331=CARTESIAN_POINT('Ctrl Pts',(-20.6931913730637,22.0591714683421,-2.40339722022666));
#40332=CARTESIAN_POINT('Ctrl Pts',(-20.6923092489605,22.0608629270598,-2.4032786460284));
#40333=CARTESIAN_POINT('Ctrl Pts',(-20.6906150823782,22.0641185112139,-2.40305071622753));
#40334=CARTESIAN_POINT('Ctrl Pts',(-20.6898028226109,22.0656825164364,-2.40294134663571));
#40335=CARTESIAN_POINT('Ctrl Pts',(-20.6878826016505,22.0693873262565,-2.40268257690375));
#40336=CARTESIAN_POINT('Ctrl Pts',(-20.6867757567197,22.0715287128677,-2.40253324807361));
#40337=CARTESIAN_POINT('Ctrl Pts',(-20.6834844793722,22.0779138215105,-2.40208869517871));
#40338=CARTESIAN_POINT('Ctrl Pts',(-20.6813070583736,22.0821611806112,-2.40179391366958));
#40339=CARTESIAN_POINT('Ctrl Pts',(-20.6612771948877,22.1214469254029,-2.39907582122423));
#40340=CARTESIAN_POINT('Ctrl Pts',(-20.6440570504599,22.1568063990951,-2.39669157176947));
#40341=CARTESIAN_POINT('Ctrl Pts',(-20.6263661435936,22.1948879917478,-2.39418024030171));
#40342=CARTESIAN_POINT('Ctrl Pts',(-20.6252477667475,22.1973032452106,-2.39402120398089));
#40343=CARTESIAN_POINT('Ctrl Pts',(-20.623591879861,22.2008909585587,-2.39378531744662));
#40344=CARTESIAN_POINT('Ctrl Pts',(-20.6230520823235,22.2020623539902,-2.3937083557285));
#40345=CARTESIAN_POINT('Ctrl Pts',(-20.621122672737,22.2062559184626,-2.39343303301176));
#40346=CARTESIAN_POINT('Ctrl Pts',(-20.6197370318817,22.2092799247597,-2.39323486423478));
#40347=CARTESIAN_POINT('Ctrl Pts',(-20.6166912817363,22.2159542009116,-2.39279828637573));
#40348=CARTESIAN_POINT('Ctrl Pts',(-20.6150332961677,22.219605440056,-2.39255997817797));
#40349=CARTESIAN_POINT('Ctrl Pts',(-20.6098935239963,22.2309806678423,-2.39181915209135));
#40350=CARTESIAN_POINT('Ctrl Pts',(-20.6064353528896,22.2387153551639,-2.39131772699228));
#40351=CARTESIAN_POINT('Ctrl Pts',(-20.601215461718,22.2505150396821,-2.39055614991386));
#40352=CARTESIAN_POINT('Ctrl Pts',(-20.5994315792356,22.2545701264949,-2.39029503054349));
#40353=CARTESIAN_POINT('Ctrl Pts',(-20.525382030641,22.4238442327912,-2.37941963746448));
#40354=CARTESIAN_POINT('Ctrl Pts',(-20.4670954225866,22.5948509486062,-2.36939932415109));
#40355=CARTESIAN_POINT('Ctrl Pts',(-20.3807777369471,22.9406995407201,-2.34947999964717));
#40356=CARTESIAN_POINT('Ctrl Pts',(-20.3522136450669,23.1147465513395,-2.3396121710883));
#40357=CARTESIAN_POINT('Ctrl Pts',(-20.3329914298302,23.3522237270046,-2.32569396876936));
#40358=CARTESIAN_POINT('Ctrl Pts',(-20.3297696829819,23.4143338821655,-2.32201463906848));
#40359=CARTESIAN_POINT('Ctrl Pts',(-20.3278485211888,23.4982554413895,-2.31697246291183));
#40360=CARTESIAN_POINT('Ctrl Pts',(-20.3275708490225,23.5200194193565,-2.31565846253371));
#40361=CARTESIAN_POINT('Ctrl Pts',(-20.3274874682947,23.5517508715871,-2.31373274017173));
#40362=CARTESIAN_POINT('Ctrl Pts',(-20.3275075141571,23.5617175807045,-2.31312645120896));
#40363=CARTESIAN_POINT('Ctrl Pts',(-20.3276262436872,23.5795711416655,-2.31203776898023));
#40364=CARTESIAN_POINT('Ctrl Pts',(-20.3277076491381,23.5874580583314,-2.31155591945637));
#40365=CARTESIAN_POINT('Ctrl Pts',(-20.3278753287331,23.5994410352372,-2.31082240163502));
#40366=CARTESIAN_POINT('Ctrl Pts',(-20.3279404627672,23.6035374005176,-2.31057139729893));
#40367=CARTESIAN_POINT('Ctrl Pts',(-20.3280674291221,23.6106672058305,-2.31013407630906));
#40368=CARTESIAN_POINT('Ctrl Pts',(-20.3281257345852,23.6137007100587,-2.30994787063113));
#40369=CARTESIAN_POINT('Ctrl Pts',(-20.328255101367,23.6199705374554,-2.3095627192955));
#40370=CARTESIAN_POINT('Ctrl Pts',(-20.3283267551518,23.6232068440057,-2.30936375522643));
#40371=CARTESIAN_POINT('Ctrl Pts',(-20.3285118830378,23.6310353026153,-2.30888208204943));
#40372=CARTESIAN_POINT('Ctrl Pts',(-20.328630299307,23.635627321483,-2.30859921796791));
#40373=CARTESIAN_POINT('Ctrl Pts',(-20.3291055775386,23.652645940715,-2.30754967485815));
#40374=CARTESIAN_POINT('Ctrl Pts',(-20.329524520711,23.6650705737708,-2.30678104831934));
#40375=CARTESIAN_POINT('Ctrl Pts',(-20.3379816248501,23.8791064406994,-2.29349794352499));
#40376=CARTESIAN_POINT('Ctrl Pts',(-20.3648620601589,24.0794869527433,-2.28037339375336));
#40377=CARTESIAN_POINT('Ctrl Pts',(-20.4236061685339,24.3336420660302,-2.26290823416026));
#40378=CARTESIAN_POINT('Ctrl Pts',(-20.4385112440124,24.3908966259931,-2.25892174635905));
#40379=CARTESIAN_POINT('Ctrl Pts',(-20.4974510269398,24.5941765230381,-2.24461605241875));
#40380=CARTESIAN_POINT('Ctrl Pts',(-20.5502629787708,24.7374509518412,-2.23423924383234));
#40381=CARTESIAN_POINT('Ctrl Pts',(-20.6402857982026,24.9368311220768,-2.21976011585997));
#40382=CARTESIAN_POINT('Ctrl Pts',(-20.6694057410358,24.9963609794146,-2.21543355863218));
#40383=CARTESIAN_POINT('Ctrl Pts',(-20.7136696199261,25.0801968853942,-2.2093774677648));
#40384=CARTESIAN_POINT('Ctrl Pts',(-20.7273323107288,25.1052618259698,-2.20757175820088));
#40385=CARTESIAN_POINT('Ctrl Pts',(-20.7435086155479,25.134022072848,-2.20550845704056));
#40386=CARTESIAN_POINT('Ctrl Pts',(-20.745698482774,25.1378966850119,-2.20523066964242));
#40387=CARTESIAN_POINT('Ctrl Pts',(-20.7490334630524,25.1437689557223,-2.20480995398076));
#40388=CARTESIAN_POINT('Ctrl Pts',(-20.7501726907364,25.1457699237998,-2.20466664733498));
#40389=CARTESIAN_POINT('Ctrl Pts',(-20.7521499520022,25.1492341949848,-2.20441863270622));
#40390=CARTESIAN_POINT('Ctrl Pts',(-20.7529869879875,25.1506980584326,-2.20431386011394));
#40391=CARTESIAN_POINT('Ctrl Pts',(-20.7547372826998,25.1537535208805,-2.20409523256723));
#40392=CARTESIAN_POINT('Ctrl Pts',(-20.7556507492884,25.1553449924254,-2.20398139181379));
#40393=CARTESIAN_POINT('Ctrl Pts',(-20.758183851802,25.1597495294493,-2.20366641880998));
#40394=CARTESIAN_POINT('Ctrl Pts',(-20.7598063850163,25.1625609394529,-2.20346547515328));
#40395=CARTESIAN_POINT('Ctrl Pts',(-20.7662052859165,25.1736099065285,-2.20267614444537));
#40396=CARTESIAN_POINT('Ctrl Pts',(-20.7710139672587,25.1818288371414,-2.20208983667212));
#40397=CARTESIAN_POINT('Ctrl Pts',(-20.8591912596,25.3310192219314,-2.19146034439946));
#40398=CARTESIAN_POINT('Ctrl Pts',(-20.9531635276924,25.4654772805208,-2.18209038457099));
#40399=CARTESIAN_POINT('Ctrl Pts',(-21.1776464334114,25.7395752964639,-2.16214986507381));
#40400=CARTESIAN_POINT('Ctrl Pts',(-21.3111478874068,25.875936023859,-2.15165689472751));
#40401=CARTESIAN_POINT('Ctrl Pts',(-21.5109245317899,26.0467497432315,-2.13664271577017));
#40402=CARTESIAN_POINT('Ctrl Pts',(-21.5675065351425,26.0919201679988,-2.13245995069935));
#40403=CARTESIAN_POINT('Ctrl Pts',(-21.6831327051265,26.1780146269689,-2.12399293140257));
#40404=CARTESIAN_POINT('Ctrl Pts',(-21.7421190237322,26.218945488239,-2.11971224727104));
#40405=CARTESIAN_POINT('Ctrl Pts',(-21.8105818006328,26.2631398676686,-2.11476567787262));
#40406=CARTESIAN_POINT('Ctrl Pts',(-21.8187679266023,26.2683719200408,-2.11417457120599));
#40407=CARTESIAN_POINT('Ctrl Pts',(-21.8335103672825,26.27770072931,-2.11311062104568));
#40408=CARTESIAN_POINT('Ctrl Pts',(-21.8400580270385,26.2818110766187,-2.11263828467855));
#40409=CARTESIAN_POINT('Ctrl Pts',(-21.8500668353751,26.288044095211,-2.11191655165509));
#40410=CARTESIAN_POINT('Ctrl Pts',(-21.8535173425892,26.2901838711706,-2.11166778764856));
#40411=CARTESIAN_POINT('Ctrl Pts',(-21.8595492099242,26.2939086719544,-2.11123300638141));
#40412=CARTESIAN_POINT('Ctrl Pts',(-21.8621287838072,26.2954965918736,-2.11104709614873));
#40413=CARTESIAN_POINT('Ctrl Pts',(-21.8674834557875,26.2987823903019,-2.110661238918));
#40414=CARTESIAN_POINT('Ctrl Pts',(-21.8702588927957,26.3004797076954,-2.11046127154123));
#40415=CARTESIAN_POINT('Ctrl Pts',(-21.8770097493999,26.3045941591153,-2.10997495048036));
#40416=CARTESIAN_POINT('Ctrl Pts',(-21.8809878342355,26.3070068875463,-2.10968843538709));
#40417=CARTESIAN_POINT('Ctrl Pts',(-21.8959417165296,26.3160322562407,-2.10861161956689));
#40418=CARTESIAN_POINT('Ctrl Pts',(-21.9069515820608,26.3225879621923,-2.10781923858378));
#40419=CARTESIAN_POINT('Ctrl Pts',(-21.9695602388023,26.3593636217945,-2.10331539435115));
#40420=CARTESIAN_POINT('Ctrl Pts',(-22.0219266568068,26.3881929669247,-2.09955607985897));
#40421=CARTESIAN_POINT('Ctrl Pts',(-22.0750363389647,26.4155369411741,-2.09574775951102));
#40422=CARTESIAN_POINT('Origin',(-23.5502525316942,23.5502525316942,-77.3107734492734));
#40423=CARTESIAN_POINT('',(-22.0750358767111,26.4155367031789,-0.597455529348901));
#40424=CARTESIAN_POINT('',(-22.0750363147453,26.4155369287046,-0.841310143832834));
#40425=CARTESIAN_POINT('',(-22.0750360153461,26.4155367745563,-77.3107734492734));
#40426=CARTESIAN_POINT('',(-26.7730021324148,23.5486483013339,-1.44183060332433));
#40427=CARTESIAN_POINT('Ctrl Pts',(-22.0750358767111,26.4155367031789,-0.597455529348901));
#40428=CARTESIAN_POINT('Ctrl Pts',(-21.9406891892397,26.3463671342851,-0.607650048982882));
#40429=CARTESIAN_POINT('Ctrl Pts',(-21.8111950680103,26.2677429624805,-0.617743844345608));
#40430=CARTESIAN_POINT('Ctrl Pts',(-21.6745161179815,26.1709367096955,-0.628341425636105));
#40431=CARTESIAN_POINT('Ctrl Pts',(-21.6615510212869,26.1616083642588,-0.629346007056065));
#40432=CARTESIAN_POINT('Ctrl Pts',(-21.6457756861704,26.1500791086699,-0.630566952953863));
#40433=CARTESIAN_POINT('Ctrl Pts',(-21.6428993559169,26.147969634968,-0.630789512356329));
#40434=CARTESIAN_POINT('Ctrl Pts',(-21.6381586429986,26.1444807217255,-0.631156228657627));
#40435=CARTESIAN_POINT('Ctrl Pts',(-21.63629224693,26.1431040449044,-0.631300576985442));
#40436=CARTESIAN_POINT('Ctrl Pts',(-21.6329601776115,26.1406407111871,-0.63155823229359));
#40437=CARTESIAN_POINT('Ctrl Pts',(-21.6314939444935,26.139554826827,-0.631671592924775));
#40438=CARTESIAN_POINT('Ctrl Pts',(-21.6283474816425,26.1372204331125,-0.631914821877224));
#40439=CARTESIAN_POINT('Ctrl Pts',(-21.6266675505145,26.1359715351094,-0.63204466191687));
#40440=CARTESIAN_POINT('Ctrl Pts',(-21.6221353912845,26.132595366367,-0.63239489012542));
#40441=CARTESIAN_POINT('Ctrl Pts',(-21.6192854567953,26.1304649994716,-0.632615060841247));
#40442=CARTESIAN_POINT('Ctrl Pts',(-21.6129963617318,26.1257475549872,-0.633100801028384));
#40443=CARTESIAN_POINT('Ctrl Pts',(-21.6095588361024,26.1231582943404,-0.63336621869832));
#40444=CARTESIAN_POINT('Ctrl Pts',(-21.5992409644101,26.1153540815471,-0.634162672166856));
#40445=CARTESIAN_POINT('Ctrl Pts',(-21.5923763096048,26.1101183093534,-0.634692286789618));
#40446=CARTESIAN_POINT('Ctrl Pts',(-21.5128320890189,26.0489416237836,-0.640827019622044));
#40447=CARTESIAN_POINT('Ctrl Pts',(-21.4425437125946,25.9899443682486,-0.646227012852222));
#40448=CARTESIAN_POINT('Ctrl Pts',(-21.0814050572507,25.6595433205295,-0.674441126662648));
#40449=CARTESIAN_POINT('Ctrl Pts',(-20.8401848157741,25.339078088967,-0.695486817408777));
#40450=CARTESIAN_POINT('Ctrl Pts',(-20.6550703130174,24.9660158531481,-0.720698091940841));
#40451=CARTESIAN_POINT('Ctrl Pts',(-20.6469204039708,24.9492265825701,-0.721832839008516));
#40452=CARTESIAN_POINT('Ctrl Pts',(-20.6363274092861,24.9269131295968,-0.723341464278263));
#40453=CARTESIAN_POINT('Ctrl Pts',(-20.6337532577105,24.9214512790999,-0.723710783115514));
#40454=CARTESIAN_POINT('Ctrl Pts',(-20.629779734269,24.9129584233236,-0.724285125859934));
#40455=CARTESIAN_POINT('Ctrl Pts',(-20.628369687679,24.9099324033173,-0.724489779711153));
#40456=CARTESIAN_POINT('Ctrl Pts',(-20.625555315277,24.9038680452123,-0.724899951916874));
#40457=CARTESIAN_POINT('Ctrl Pts',(-20.6241510159881,24.9008296993541,-0.725105470878797));
#40458=CARTESIAN_POINT('Ctrl Pts',(-20.6210253847441,24.8940393171884,-0.72556482186619));
#40459=CARTESIAN_POINT('Ctrl Pts',(-20.6193065255384,24.8902861551695,-0.725818738859921));
#40460=CARTESIAN_POINT('Ctrl Pts',(-20.6142975237022,24.8792931608235,-0.726562542065408));
#40461=CARTESIAN_POINT('Ctrl Pts',(-20.6110269792714,24.8720444793915,-0.727053102533168));
#40462=CARTESIAN_POINT('Ctrl Pts',(-20.5871629283512,24.8186267815638,-0.7306690533251));
#40463=CARTESIAN_POINT('Ctrl Pts',(-20.5676324657403,24.7719932194257,-0.733830681566581));
#40464=CARTESIAN_POINT('Ctrl Pts',(-20.5073010873557,24.6178586070316,-0.744304580837282));
#40465=CARTESIAN_POINT('Ctrl Pts',(-20.4711581791909,24.5086413524432,-0.751767525059768));
#40466=CARTESIAN_POINT('Ctrl Pts',(-20.3526157163248,24.0737225703439,-0.781600810601189));
#40467=CARTESIAN_POINT('Ctrl Pts',(-20.315494250577,23.7379292830332,-0.805123472645065));
#40468=CARTESIAN_POINT('Ctrl Pts',(-20.3312613925392,23.3944373816574,-0.826868117253289));
#40469=CARTESIAN_POINT('Ctrl Pts',(-20.3316604864376,23.3864002680407,-0.827375460647435));
#40470=CARTESIAN_POINT('Ctrl Pts',(-20.3325564618243,23.3696254120253,-0.828431242859504));
#40471=CARTESIAN_POINT('Ctrl Pts',(-20.3330588423977,23.3608880043832,-0.828979386343283));
#40472=CARTESIAN_POINT('Ctrl Pts',(-20.3337894704851,23.3490243991397,-0.829721142296514));
#40473=CARTESIAN_POINT('Ctrl Pts',(-20.3339866890196,23.3458964334275,-0.829916477037895));
#40474=CARTESIAN_POINT('Ctrl Pts',(-20.3343051639504,23.3409599716785,-0.830224368877319));
#40475=CARTESIAN_POINT('Ctrl Pts',(-20.3344233828609,23.3391512921675,-0.83033709750462));
#40476=CARTESIAN_POINT('Ctrl Pts',(-20.3346648922272,23.3355036260952,-0.830564280117797));
#40477=CARTESIAN_POINT('Ctrl Pts',(-20.3347882335411,23.3336646583821,-0.83067872994329));
#40478=CARTESIAN_POINT('Ctrl Pts',(-20.3350746513123,23.3294484607367,-0.830940937423881));
#40479=CARTESIAN_POINT('Ctrl Pts',(-20.3352387865152,23.3270713079165,-0.831088634373186));
#40480=CARTESIAN_POINT('Ctrl Pts',(-20.3355888746903,23.322081554044,-0.831398368553348));
#40481=CARTESIAN_POINT('Ctrl Pts',(-20.3357753766395,23.3194689914439,-0.831560374770081));
#40482=CARTESIAN_POINT('Ctrl Pts',(-20.3362768529567,23.3125627469246,-0.831988201876065));
#40483=CARTESIAN_POINT('Ctrl Pts',(-20.3365972477742,23.3082694456398,-0.832253720882407));
#40484=CARTESIAN_POINT('Ctrl Pts',(-20.3375863336016,23.2953641744624,-0.833050552740466));
#40485=CARTESIAN_POINT('Ctrl Pts',(-20.3382810523757,23.2867541541111,-0.833580442814485));
#40486=CARTESIAN_POINT('Ctrl Pts',(-20.3408866088912,23.2560047962555,-0.835467002141052));
#40487=CARTESIAN_POINT('Ctrl Pts',(-20.3429918478851,23.233881983798,-0.836813438138309));
#40488=CARTESIAN_POINT('Ctrl Pts',(-20.354412246798,23.1257439264778,-0.843349452674268));
#40489=CARTESIAN_POINT('Ctrl Pts',(-20.3669604263103,23.0400990174421,-0.848385321555301));
#40490=CARTESIAN_POINT('Ctrl Pts',(-20.4356552978211,22.6745422818763,-0.869663373985702));
#40491=CARTESIAN_POINT('Ctrl Pts',(-20.5253974447585,22.4022763627015,-0.885077981120781));
#40492=CARTESIAN_POINT('Ctrl Pts',(-20.6605133533898,22.1233238076916,-0.903067437832979));
#40493=CARTESIAN_POINT('Ctrl Pts',(-20.6714470862214,22.1013918524545,-0.904496619908667));
#40494=CARTESIAN_POINT('Ctrl Pts',(-20.6909882385076,22.0632889276861,-0.907007288038405));
#40495=CARTESIAN_POINT('Ctrl Pts',(-20.6994854571633,22.0470625482935,-0.908085382973898));
#40496=CARTESIAN_POINT('Ctrl Pts',(-20.7102045944783,22.0270109813662,-0.909429191375002));
#40497=CARTESIAN_POINT('Ctrl Pts',(-20.7122967813345,22.0231165635955,-0.909690731045899));
#40498=CARTESIAN_POINT('Ctrl Pts',(-20.7162993374321,22.0157027962459,-0.910189670847715));
#40499=CARTESIAN_POINT('Ctrl Pts',(-20.718208267084,22.012182676025,-0.91042702391303));
#40500=CARTESIAN_POINT('Ctrl Pts',(-20.72269401461,22.003947494906,-0.91098337019839));
#40501=CARTESIAN_POINT('Ctrl Pts',(-20.7252760685309,21.9992353117997,-0.911302534550945));
#40502=CARTESIAN_POINT('Ctrl Pts',(-20.7311938006479,21.9884993996366,-0.912031593763147));
#40503=CARTESIAN_POINT('Ctrl Pts',(-20.7345370160915,21.9824798732024,-0.912441738014669));
#40504=CARTESIAN_POINT('Ctrl Pts',(-20.7394294034469,21.9737371592558,-0.913039446104469));
#40505=CARTESIAN_POINT('Ctrl Pts',(-20.7409633103103,21.9710054172945,-0.913226493134887));
#40506=CARTESIAN_POINT('Ctrl Pts',(-20.7431076351569,21.9671995892408,-0.913487488154249));
#40507=CARTESIAN_POINT('Ctrl Pts',(-20.7437146943713,21.9661236049858,-0.913561321737854));
#40508=CARTESIAN_POINT('Ctrl Pts',(-20.747695947375,21.9590764905902,-0.914045187491566));
#40509=CARTESIAN_POINT('Ctrl Pts',(-20.7510885576144,21.9531158289558,-0.914455847506404));
#40510=CARTESIAN_POINT('Ctrl Pts',(-20.7575034365023,21.9419284018101,-0.915229256616018));
#40511=CARTESIAN_POINT('Ctrl Pts',(-20.7605214202229,21.9366992042798,-0.915591855986747));
#40512=CARTESIAN_POINT('Ctrl Pts',(-20.7763256130222,21.9094924909312,-0.917484170986884));
#40513=CARTESIAN_POINT('Ctrl Pts',(-20.7893566147258,21.8876588530324,-0.919022436824428));
#40514=CARTESIAN_POINT('Ctrl Pts',(-20.8080175080907,21.8572166955915,-0.921195966161289));
#40515=CARTESIAN_POINT('Ctrl Pts',(-20.8134325600513,21.8484770747166,-0.921823334741975));
#40516=CARTESIAN_POINT('Ctrl Pts',(-20.8210792677051,21.8362665682698,-0.922704651194728));
#40517=CARTESIAN_POINT('Ctrl Pts',(-20.8232759508806,21.8327737646856,-0.922957303365962));
#40518=CARTESIAN_POINT('Ctrl Pts',(-20.8273096031884,21.8263873635396,-0.923420280947412));
#40519=CARTESIAN_POINT('Ctrl Pts',(-20.8291444949307,21.8234924551346,-0.923630528991319));
#40520=CARTESIAN_POINT('Ctrl Pts',(-20.8328635724077,21.8176455159188,-0.924055952912407));
#40521=CARTESIAN_POINT('Ctrl Pts',(-20.8347479583385,21.8146936190968,-0.924271136033673));
#40522=CARTESIAN_POINT('Ctrl Pts',(-20.8393828470093,21.8074590782071,-0.924799501662318));
#40523=CARTESIAN_POINT('Ctrl Pts',(-20.8421386842436,21.803179877901,-0.925112883111043));
#40524=CARTESIAN_POINT('Ctrl Pts',(-20.8521345947711,21.7877389390363,-0.92624678959131));
#40525=CARTESIAN_POINT('Ctrl Pts',(-20.8594335547906,21.7766156492251,-0.927069519156938));
#40526=CARTESIAN_POINT('Ctrl Pts',(-20.9638966458085,21.619547598452,-0.938771732582543));
#40527=CARTESIAN_POINT('Ctrl Pts',(-21.0727263883099,21.4817496818975,-0.950105527629853));
#40528=CARTESIAN_POINT('Ctrl Pts',(-21.2162719445651,21.3276641619678,-0.964114602848038));
#40529=CARTESIAN_POINT('Ctrl Pts',(-21.240763950178,21.3022252100691,-0.966474950371078));
#40530=CARTESIAN_POINT('Ctrl Pts',(-21.4640350960089,21.0778219452219,-0.987714141418737));
#40531=CARTESIAN_POINT('Ctrl Pts',(-21.6876485439697,20.9052693749875,-1.00718131785204));
#40532=CARTESIAN_POINT('Ctrl Pts',(-21.9451020023631,20.755635931005,-1.02603150631787));
#40533=CARTESIAN_POINT('Ctrl Pts',(-21.9594407340496,20.7474489319291,-1.02707029475024));
#40534=CARTESIAN_POINT('Ctrl Pts',(-21.9769908604176,20.7376063916341,-1.02832771836351));
#40535=CARTESIAN_POINT('Ctrl Pts',(-21.9801425929372,20.7358457778589,-1.02855298473468));
#40536=CARTESIAN_POINT('Ctrl Pts',(-21.9853356326806,20.7329562918876,-1.0289232421387));
#40537=CARTESIAN_POINT('Ctrl Pts',(-21.9873752073292,20.7318243398283,-1.02906843100839));
#40538=CARTESIAN_POINT('Ctrl Pts',(-21.9909596219089,20.729840097868,-1.02932318390013));
#40539=CARTESIAN_POINT('Ctrl Pts',(-21.9925039301707,20.728986863613,-1.02943280906032));
#40540=CARTESIAN_POINT('Ctrl Pts',(-21.9958558592982,20.7271385054723,-1.02967046320114));
#40541=CARTESIAN_POINT('Ctrl Pts',(-21.9976637312556,20.7261438515941,-1.02979846149781));
#40542=CARTESIAN_POINT('Ctrl Pts',(-22.0024749013599,20.7235028611883,-1.03013861681776));
#40543=CARTESIAN_POINT('Ctrl Pts',(-22.0054798812383,20.7218595690153,-1.03035057745891));
#40544=CARTESIAN_POINT('Ctrl Pts',(-22.0120955278317,20.7182554491524,-1.03081614673436));
#40545=CARTESIAN_POINT('Ctrl Pts',(-22.0157073431359,20.7162967259754,-1.03106962177661));
#40546=CARTESIAN_POINT('Ctrl Pts',(-22.0264533675234,20.7104956177878,-1.03182171458604));
#40547=CARTESIAN_POINT('Ctrl Pts',(-22.0335983977896,20.7066731914664,-1.03231909230179));
#40548=CARTESIAN_POINT('Ctrl Pts',(-22.0587590609275,20.6933346289821,-1.03406140800573));
#40549=CARTESIAN_POINT('Ctrl Pts',(-22.0768508757845,20.6839621967392,-1.03529777707063));
#40550=CARTESIAN_POINT('Ctrl Pts',(-22.1319873841863,20.6560588418074,-1.03901978519361));
#40551=CARTESIAN_POINT('Ctrl Pts',(-22.1693028278144,20.6380692630539,-1.04147649304671));
#40552=CARTESIAN_POINT('Ctrl Pts',(-22.3056852475059,20.5755312400114,-1.05026862483504));
#40553=CARTESIAN_POINT('Ctrl Pts',(-22.4066469985118,20.5352758713674,-1.05642738341751));
#40554=CARTESIAN_POINT('Ctrl Pts',(-22.7189746396144,20.4286976879988,-1.07496349951045));
#40555=CARTESIAN_POINT('Ctrl Pts',(-22.9352908868415,20.3789837441137,-1.08715031691132));
#40556=CARTESIAN_POINT('Ctrl Pts',(-23.1807716990753,20.3486472796386,-1.10148829916147));
#40557=CARTESIAN_POINT('Ctrl Pts',(-23.2065879277729,20.3457733435946,-1.10300162827251));
#40558=CARTESIAN_POINT('Ctrl Pts',(-23.2526112274924,20.3412124463707,-1.10571127670561));
#40559=CARTESIAN_POINT('Ctrl Pts',(-23.2728049353553,20.3394035129084,-1.10690422144167));
#40560=CARTESIAN_POINT('Ctrl Pts',(-23.2976821369309,20.3374114698292,-1.10837941269145));
#40561=CARTESIAN_POINT('Ctrl Pts',(-23.30235100065,20.3370478504293,-1.1086565122514));
#40562=CARTESIAN_POINT('Ctrl Pts',(-23.3110498499032,20.3363894407713,-1.10917325315885));
#40563=CARTESIAN_POINT('Ctrl Pts',(-23.3150796334605,20.336092050651,-1.10941281949309));
#40564=CARTESIAN_POINT('Ctrl Pts',(-23.3229245049975,20.3355279467843,-1.10987955315879));
#40565=CARTESIAN_POINT('Ctrl Pts',(-23.326739530678,20.3352604435634,-1.1101066972761));
#40566=CARTESIAN_POINT('Ctrl Pts',(-23.3833570608287,20.3313917801237,-1.11348020019779));
#40567=CARTESIAN_POINT('Ctrl Pts',(-23.4362374200321,20.3290852448379,-1.11666391026));
#40568=CARTESIAN_POINT('Ctrl Pts',(-23.497878471502,20.3279163042374,-1.12042104157735));
#40569=CARTESIAN_POINT('Ctrl Pts',(-23.5066091630582,20.3277862310213,-1.12095426105015));
#40570=CARTESIAN_POINT('Ctrl Pts',(-23.5196278613997,20.3276451900846,-1.12175099456063));
#40571=CARTESIAN_POINT('Ctrl Pts',(-23.5239155864056,20.3276072962303,-1.1220136629853));
#40572=CARTESIAN_POINT('Ctrl Pts',(-23.5315658050816,20.3275549543021,-1.12248279392042));
#40573=CARTESIAN_POINT('Ctrl Pts',(-23.5349282760058,20.3275372113267,-1.12268915268429));
#40574=CARTESIAN_POINT('Ctrl Pts',(-23.5420200070604,20.3275108890047,-1.12312472780098));
#40575=CARTESIAN_POINT('Ctrl Pts',(-23.545749264336,20.3275035203091,-1.1233539818622));
#40576=CARTESIAN_POINT('Ctrl Pts',(-23.5556055621826,20.3275011530905,-1.12396043196195));
#40577=CARTESIAN_POINT('Ctrl Pts',(-23.561732568387,20.327517154541,-1.124337972828));
#40578=CARTESIAN_POINT('Ctrl Pts',(-23.5895106302914,20.3276689173489,-1.12605216208167));
#40579=CARTESIAN_POINT('Ctrl Pts',(-23.6111596215759,20.3280053904425,-1.12739509630084));
#40580=CARTESIAN_POINT('Ctrl Pts',(-23.7702022688411,20.3320805995236,-1.13731393118291));
#40581=CARTESIAN_POINT('Ctrl Pts',(-23.9072165014444,20.3443866249787,-1.14615936893646));
#40582=CARTESIAN_POINT('Ctrl Pts',(-24.0816243669733,20.3713709488588,-1.15780325421886));
#40583=CARTESIAN_POINT('Ctrl Pts',(-24.1201236074863,20.3780465249892,-1.16039726135637));
#40584=CARTESIAN_POINT('Ctrl Pts',(-24.1887013527223,20.3912262513658,-1.16505732630796));
#40585=CARTESIAN_POINT('Ctrl Pts',(-24.2188265272765,20.3974644495236,-1.16711813021863));
#40586=CARTESIAN_POINT('Ctrl Pts',(-24.2737318902162,20.4096563409319,-1.17089712014989));
#40587=CARTESIAN_POINT('Ctrl Pts',(-24.2985398455746,20.4154745670875,-1.17261324690678));
#40588=CARTESIAN_POINT('Ctrl Pts',(-24.3443584746063,20.4267953253297,-1.17579742845327));
#40589=CARTESIAN_POINT('Ctrl Pts',(-24.3653876833665,20.4322172779897,-1.17726460484576));
#40590=CARTESIAN_POINT('Ctrl Pts',(-24.4045734455441,20.44274404526,-1.18000824153349));
#40591=CARTESIAN_POINT('Ctrl Pts',(-24.4227431777805,20.4477965229126,-1.18128434308218));
#40592=CARTESIAN_POINT('Ctrl Pts',(-24.4568296556016,20.4575981152262,-1.18368494701112));
#40593=CARTESIAN_POINT('Ctrl Pts',(-24.4727561152681,20.4623113794935,-1.18480933968115));
#40594=CARTESIAN_POINT('Ctrl Pts',(-24.6372351010361,20.5123732204015,-1.19644671620746));
#40595=CARTESIAN_POINT('Ctrl Pts',(-24.7823733402676,20.5682854026854,-1.20694128480268));
#40596=CARTESIAN_POINT('Ctrl Pts',(-24.9677942310842,20.6555759029267,-1.22022291435769));
#40597=CARTESIAN_POINT('Ctrl Pts',(-25.0121754102516,20.6777345716642,-1.22339090242088));
#40598=CARTESIAN_POINT('Ctrl Pts',(-25.0609626632634,20.7035169305174,-1.22684658699875));
#40599=CARTESIAN_POINT('Ctrl Pts',(-25.065888267137,20.7061363239429,-1.22719516660556));
#40600=CARTESIAN_POINT('Ctrl Pts',(-25.0728443316413,20.7098587012378,-1.22768697476471));
#40601=CARTESIAN_POINT('Ctrl Pts',(-25.0748804097663,20.7109510797789,-1.22783087322785));
#40602=CARTESIAN_POINT('Ctrl Pts',(-25.0785980496897,20.7129507869062,-1.22809350924025));
#40603=CARTESIAN_POINT('Ctrl Pts',(-25.0802799814418,20.7138574223293,-1.22821229122766));
#40604=CARTESIAN_POINT('Ctrl Pts',(-25.0835018178565,20.7155978339504,-1.22843974754709));
#40605=CARTESIAN_POINT('Ctrl Pts',(-25.0850418488813,20.7164313692279,-1.22854843732257));
#40606=CARTESIAN_POINT('Ctrl Pts',(-25.0889416553437,20.7185462344983,-1.22882358756877));
#40607=CARTESIAN_POINT('Ctrl Pts',(-25.0913005160186,20.7198292624725,-1.22898993873865));
#40608=CARTESIAN_POINT('Ctrl Pts',(-25.0993892850173,20.7242420029142,-1.22956011566033));
#40609=CARTESIAN_POINT('Ctrl Pts',(-25.105111333713,20.7273862052771,-1.22996301802266));
#40610=CARTESIAN_POINT('Ctrl Pts',(-25.1188017422576,20.7349631897336,-1.23092601945571));
#40611=CARTESIAN_POINT('Ctrl Pts',(-25.1267609731641,20.7394124715891,-1.23148509062852));
#40612=CARTESIAN_POINT('Ctrl Pts',(-25.1555292912804,20.7556548551948,-1.23350335149589));
#40613=CARTESIAN_POINT('Ctrl Pts',(-25.1762263928661,20.7676460689092,-1.23495065176322));
#40614=CARTESIAN_POINT('Ctrl Pts',(-25.2659516747629,20.8209729160657,-1.24121279745851));
#40615=CARTESIAN_POINT('Ctrl Pts',(-25.3335566898949,20.8646577918024,-1.24589971744871));
#40616=CARTESIAN_POINT('Ctrl Pts',(-25.5369947641291,21.0071887534181,-1.26013048621562));
#40617=CARTESIAN_POINT('Ctrl Pts',(-25.6667930128477,21.1141532379139,-1.26940474851507));
#40618=CARTESIAN_POINT('Ctrl Pts',(-25.8927779845824,21.3321407140563,-1.2870110877469));
#40619=CARTESIAN_POINT('Ctrl Pts',(-25.9908668450641,21.4405507302487,-1.29528699558577));
#40620=CARTESIAN_POINT('Ctrl Pts',(-26.0915456383318,21.5682780255872,-1.30482584102547));
#40621=CARTESIAN_POINT('Ctrl Pts',(-26.1017294128243,21.5814053289098,-1.30580374199393));
#40622=CARTESIAN_POINT('Ctrl Pts',(-26.1516974453986,21.6468549604466,-1.31066854642246));
#40623=CARTESIAN_POINT('Ctrl Pts',(-26.1899737391699,21.7003041654103,-1.31460798484887));
#40624=CARTESIAN_POINT('Ctrl Pts',(-26.2312545835782,21.761841015329,-1.31912179449434));
#40625=CARTESIAN_POINT('Ctrl Pts',(-26.2358947417348,21.768816686193,-1.31963315486224));
#40626=CARTESIAN_POINT('Ctrl Pts',(-26.2428650542993,21.7793844683761,-1.3204073972785));
#40627=CARTESIAN_POINT('Ctrl Pts',(-26.2452153620788,21.7829632975486,-1.32066952185399));
#40628=CARTESIAN_POINT('Ctrl Pts',(-26.2492847572197,21.7891867868779,-1.32112522185629));
#40629=CARTESIAN_POINT('Ctrl Pts',(-26.2510071109343,21.7918293134111,-1.32131867463097));
#40630=CARTESIAN_POINT('Ctrl Pts',(-26.2545858154601,21.7973376131846,-1.3217218427001));
#40631=CARTESIAN_POINT('Ctrl Pts',(-26.2564414958837,21.8002038148934,-1.3219315826948));
#40632=CARTESIAN_POINT('Ctrl Pts',(-26.2608058199096,21.8069682966453,-1.32242648300178));
#40633=CARTESIAN_POINT('Ctrl Pts',(-26.2633106093111,21.8108690433443,-1.32271178660218));
#40634=CARTESIAN_POINT('Ctrl Pts',(-26.2714956187075,21.823676377488,-1.32364826854078));
#40635=CARTESIAN_POINT('Ctrl Pts',(-26.2771404191291,21.8326054200945,-1.32430076179848));
#40636=CARTESIAN_POINT('Ctrl Pts',(-26.3572880787015,21.9607752441523,-1.33366150852107));
#40637=CARTESIAN_POINT('Ctrl Pts',(-26.4239429853942,22.0847219040408,-1.34265862620585));
#40638=CARTESIAN_POINT('Ctrl Pts',(-26.6040659631666,22.4795408494138,-1.37118337491613));
#40639=CARTESIAN_POINT('Ctrl Pts',(-26.6888076315404,22.7618100676,-1.39152292120949));
#40640=CARTESIAN_POINT('Ctrl Pts',(-26.73606606423,23.0635739890314,-1.41158869683743));
#40641=CARTESIAN_POINT('Ctrl Pts',(-26.7378702580484,23.0755346090853,-1.41238107168448));
#40642=CARTESIAN_POINT('Ctrl Pts',(-26.7410447006124,23.0974135554134,-1.41382482055198));
#40643=CARTESIAN_POINT('Ctrl Pts',(-26.7424361439456,23.107328617316,-1.41447696056039));
#40644=CARTESIAN_POINT('Ctrl Pts',(-26.7449193965863,23.1256433855745,-1.41567744416891));
#40645=CARTESIAN_POINT('Ctrl Pts',(-26.7460243371001,23.1340411967884,-1.41622629886083));
#40646=CARTESIAN_POINT('Ctrl Pts',(-26.7528256392466,23.1873570625371,-1.41970031813369));
#40647=CARTESIAN_POINT('Ctrl Pts',(-26.7576083312586,23.2323894647162,-1.42258720363565));
#40648=CARTESIAN_POINT('Ctrl Pts',(-26.7618608959266,23.2824579619789,-1.42573349632634));
#40649=CARTESIAN_POINT('Ctrl Pts',(-26.762269679851,23.287406459806,-1.42604377223927));
#40650=CARTESIAN_POINT('Ctrl Pts',(-26.762863805056,23.2948070085089,-1.42650674789126));
#40651=CARTESIAN_POINT('Ctrl Pts',(-26.7630577767862,23.2972583296754,-1.42665993006355));
#40652=CARTESIAN_POINT('Ctrl Pts',(-26.7633869324547,23.3014794711676,-1.42692340942656));
#40653=CARTESIAN_POINT('Ctrl Pts',(-26.7635234598359,23.3032491807273,-1.42703378265865));
#40654=CARTESIAN_POINT('Ctrl Pts',(-26.7637944697061,23.3068003458606,-1.42725507940636));
#40655=CARTESIAN_POINT('Ctrl Pts',(-26.7639289326623,23.3085817969736,-1.42736600128482));
#40656=CARTESIAN_POINT('Ctrl Pts',(-26.7641997370059,23.312209778776,-1.42759171088979));
#40657=CARTESIAN_POINT('Ctrl Pts',(-26.7643359686806,23.314056319026,-1.42770649246917));
#40658=CARTESIAN_POINT('Ctrl Pts',(-26.7646473351462,23.3183268615568,-1.42797172582079));
#40659=CARTESIAN_POINT('Ctrl Pts',(-26.7648213197668,23.3207509505021,-1.4281221126366));
#40660=CARTESIAN_POINT('Ctrl Pts',(-26.7652640380277,23.3270185262977,-1.42851051552325));
#40661=CARTESIAN_POINT('Ctrl Pts',(-26.7655286226081,23.3308623163659,-1.42874829986085));
#40662=CARTESIAN_POINT('Ctrl Pts',(-26.7705596293757,23.4059153305016,-1.43338326392699));
#40663=CARTESIAN_POINT('Ctrl Pts',(-26.7729666008245,23.4772686408052,-1.43764991829428));
#40664=CARTESIAN_POINT('Ctrl Pts',(-26.7730021324148,23.5486483013339,-1.44183060332433));
#40665=CARTESIAN_POINT('Ctrl Pts',(-26.7730021302442,23.5486439466878,-1.44183034827392));
#40666=CARTESIAN_POINT('Ctrl Pts',(-26.7731688677631,23.882697335105,-1.4613957704159));
#40667=CARTESIAN_POINT('Ctrl Pts',(-26.7214006904693,24.2147936159358,-1.4791387893778));
#40668=CARTESIAN_POINT('Ctrl Pts',(-26.5997245547146,24.5947803069446,-1.502308737071));
#40669=CARTESIAN_POINT('Ctrl Pts',(-26.5781038952386,24.6558895429473,-1.50612049904104));
#40670=CARTESIAN_POINT('Ctrl Pts',(-26.5386957085977,24.7574273031958,-1.51262655607523));
#40671=CARTESIAN_POINT('Ctrl Pts',(-26.521892637583,24.7982182115299,-1.5152882471269));
#40672=CARTESIAN_POINT('Ctrl Pts',(-26.5011905884798,24.8456833586222,-1.51844656978587));
#40673=CARTESIAN_POINT('Ctrl Pts',(-26.4980978445266,24.8527057755179,-1.51891542690475));
#40674=CARTESIAN_POINT('Ctrl Pts',(-26.4933267199962,24.8634350940985,-1.51963423409926));
#40675=CARTESIAN_POINT('Ctrl Pts',(-26.4916663343527,24.8671500073321,-1.51988356550995));
#40676=CARTESIAN_POINT('Ctrl Pts',(-26.4886287816072,24.8739117613638,-1.52033821790734));
#40677=CARTESIAN_POINT('Ctrl Pts',(-26.487253898034,24.876959626846,-1.5205434600195));
#40678=CARTESIAN_POINT('Ctrl Pts',(-26.4844828434696,24.8830771307915,-1.52095603030087));
#40679=CARTESIAN_POINT('Ctrl Pts',(-26.4830865927558,24.8861467283428,-1.52116336102295));
#40680=CARTESIAN_POINT('Ctrl Pts',(-26.4791071873032,24.8948589726428,-1.52175271090289));
#40681=CARTESIAN_POINT('Ctrl Pts',(-26.4765125588,24.9004963347251,-1.52213512622008));
#40682=CARTESIAN_POINT('Ctrl Pts',(-26.46548954095,24.9242650965224,-1.52375205096208));
#40683=CARTESIAN_POINT('Ctrl Pts',(-26.4569089360643,24.9423250392733,-1.52499182731233));
#40684=CARTESIAN_POINT('Ctrl Pts',(-26.2795236178546,25.3068837479351,-1.55025027321395));
#40685=CARTESIAN_POINT('Ctrl Pts',(-26.05009296358,25.6203481629741,-1.57680513659364));
#40686=CARTESIAN_POINT('Ctrl Pts',(-25.7261133975403,25.9283973336497,-1.60659851310883));
#40687=CARTESIAN_POINT('Ctrl Pts',(-25.6800690334475,25.9697206084309,-1.61067861131474));
#40688=CARTESIAN_POINT('Ctrl Pts',(-25.6064119191038,26.0320920352255,-1.61693537097136));
#40689=CARTESIAN_POINT('Ctrl Pts',(-25.5796017479016,26.0540617753315,-1.61915967689));
#40690=CARTESIAN_POINT('Ctrl Pts',(-25.5430636961239,26.0830305399558,-1.62211471480445));
#40691=CARTESIAN_POINT('Ctrl Pts',(-25.5336447073969,26.090413208489,-1.62286980226507));
#40692=CARTESIAN_POINT('Ctrl Pts',(-25.5198596502624,26.1010946078229,-1.62396494125104));
#40693=CARTESIAN_POINT('Ctrl Pts',(-25.5155260913321,26.1044348540204,-1.62430779354336));
#40694=CARTESIAN_POINT('Ctrl Pts',(-25.5077496738672,26.1103972989696,-1.62492045489268));
#40695=CARTESIAN_POINT('Ctrl Pts',(-25.5043100136147,26.1130236195785,-1.6251905492195));
#40696=CARTESIAN_POINT('Ctrl Pts',(-25.4990630010683,26.1170132220948,-1.62560118456961));
#40697=CARTESIAN_POINT('Ctrl Pts',(-25.4972595025747,26.1183815282102,-1.62574208048134));
#40698=CARTESIAN_POINT('Ctrl Pts',(-25.4939724484223,26.1208699484578,-1.62599842485238));
#40699=CARTESIAN_POINT('Ctrl Pts',(-25.4924893693122,26.1219906763563,-1.6261139168333));
#40700=CARTESIAN_POINT('Ctrl Pts',(-25.4892842238448,26.1244083752498,-1.62636314967497));
#40701=CARTESIAN_POINT('Ctrl Pts',(-25.4875618302637,26.1257048981374,-1.62649685854838));
#40702=CARTESIAN_POINT('Ctrl Pts',(-25.4829003699228,26.1292064661729,-1.62685812255144));
#40703=CARTESIAN_POINT('Ctrl Pts',(-25.4799588197479,26.1314082234219,-1.62708544526047));
#40704=CARTESIAN_POINT('Ctrl Pts',(-25.4662239345746,26.1416522150239,-1.62814389137584));
#40705=CARTESIAN_POINT('Ctrl Pts',(-25.4553838437218,26.1496319642393,-1.62897067962835));
#40706=CARTESIAN_POINT('Ctrl Pts',(-25.4433578199757,26.1583690746709,-1.62987887947253));
#40707=CARTESIAN_POINT('Ctrl Pts',(-25.4422212456592,26.1591936808315,-1.6299646243613));
#40708=CARTESIAN_POINT('Ctrl Pts',(-25.4340174663101,26.1651374976655,-1.63058289324737));
#40709=CARTESIAN_POINT('Ctrl Pts',(-25.4269299474096,26.170228790237,-1.63111362986479));
#40710=CARTESIAN_POINT('Ctrl Pts',(-25.415555145862,26.1783299958641,-1.63196012980029));
#40711=CARTESIAN_POINT('Ctrl Pts',(-25.4112811118018,26.1813583115683,-1.6322770127559));
#40712=CARTESIAN_POINT('Ctrl Pts',(-25.3160731870645,26.2484686922482,-1.63930999773033));
#40713=CARTESIAN_POINT('Ctrl Pts',(-25.221879049007,26.3078172271735,-1.64574545177314));
#40714=CARTESIAN_POINT('Ctrl Pts',(-25.0677921524255,26.3940983649729,-1.65577689716675));
#40715=CARTESIAN_POINT('Ctrl Pts',(-25.0098309996988,26.4242770148866,-1.65944560441169));
#40716=CARTESIAN_POINT('Ctrl Pts',(-24.8384490518839,26.5069877379262,-1.67009704450526));
#40717=CARTESIAN_POINT('Ctrl Pts',(-24.7228437804965,26.5547096218153,-1.67704280289335));
#40718=CARTESIAN_POINT('Ctrl Pts',(-24.4809946756595,26.6384545569573,-1.69152440631513));
#40719=CARTESIAN_POINT('Ctrl Pts',(-24.354741598107,26.6737225150426,-1.69906009168216));
#40720=CARTESIAN_POINT('Ctrl Pts',(-24.1731414815125,26.7127085089994,-1.71009704194022));
#40721=CARTESIAN_POINT('Ctrl Pts',(-24.1192996560617,26.7228387428969,-1.71339236847744));
#40722=CARTESIAN_POINT('Ctrl Pts',(-24.0572202712967,26.7328877732047,-1.71722660705486));
#40723=CARTESIAN_POINT('Ctrl Pts',(-24.0492075501952,26.7341537954143,-1.717722156424));
#40724=CARTESIAN_POINT('Ctrl Pts',(-24.0370773565378,26.7360234697395,-1.71847337212975));
#40725=CARTESIAN_POINT('Ctrl Pts',(-24.0329633126662,26.7366494281045,-1.71872832969818));
#40726=CARTESIAN_POINT('Ctrl Pts',(-24.0258503815691,26.7377175803746,-1.71916944620626));
#40727=CARTESIAN_POINT('Ctrl Pts',(-24.0228520544526,26.7381635157638,-1.71935548613726));
#40728=CARTESIAN_POINT('Ctrl Pts',(-24.0166426101538,26.739078081662,-1.71974096822388));
#40729=CARTESIAN_POINT('Ctrl Pts',(-24.0134314064034,26.7395460934891,-1.71994042979302));
#40730=CARTESIAN_POINT('Ctrl Pts',(-24.005643549946,26.7406691123034,-1.72042443636991));
#40731=CARTESIAN_POINT('Ctrl Pts',(-24.0010661933281,26.7413191213266,-1.72070913959362));
#40732=CARTESIAN_POINT('Ctrl Pts',(-23.9839850241543,26.7437072525439,-1.72177240947607));
#40733=CARTESIAN_POINT('Ctrl Pts',(-23.9714725588401,26.745381732615,-1.72255298992911));
#40734=CARTESIAN_POINT('Ctrl Pts',(-23.7548825809245,26.7730725068247,-1.73609516435349));
#40735=CARTESIAN_POINT('Ctrl Pts',(-23.5488261779048,26.7795575172112,-1.74949223434172));
#40736=CARTESIAN_POINT('Ctrl Pts',(-23.1585547512216,26.754479492105,-1.775700621787));
#40737=CARTESIAN_POINT('Ctrl Pts',(-22.974894936122,26.7266434606477,-1.78838123610047));
#40738=CARTESIAN_POINT('Ctrl Pts',(-22.7524258049084,26.672987974116,-1.80364754112412));
#40739=CARTESIAN_POINT('Ctrl Pts',(-22.7104104384663,26.6619513714923,-1.80652510275852));
#40740=CARTESIAN_POINT('Ctrl Pts',(-22.6230729215237,26.6371115853815,-1.81247862326149));
#40741=CARTESIAN_POINT('Ctrl Pts',(-22.5778047791555,26.6231512822985,-1.81554834664257));
#40742=CARTESIAN_POINT('Ctrl Pts',(-22.5164159832112,26.6027269101449,-1.81967421457841));
#40743=CARTESIAN_POINT('Ctrl Pts',(-22.5000175781196,26.5971237814988,-1.82077267017262));
#40744=CARTESIAN_POINT('Ctrl Pts',(-22.4768789995183,26.5890086149181,-1.82231663301923));
#40745=CARTESIAN_POINT('Ctrl Pts',(-22.4701011524368,26.5866059816586,-1.8227681662272));
#40746=CARTESIAN_POINT('Ctrl Pts',(-22.4597853303753,26.5829102824631,-1.82345421925334));
#40747=CARTESIAN_POINT('Ctrl Pts',(-22.4562415407407,26.5816336859645,-1.82368968666073));
#40748=CARTESIAN_POINT('Ctrl Pts',(-22.4496978566411,26.5792634535825,-1.82412407941771));
#40749=CARTESIAN_POINT('Ctrl Pts',(-22.4466973393016,26.5781715687978,-1.82432310752258));
#40750=CARTESIAN_POINT('Ctrl Pts',(-22.4418114825409,26.5763853839519,-1.82464693117836));
#40751=CARTESIAN_POINT('Ctrl Pts',(-22.4399251701813,26.5756937803868,-1.82477188818677));
#40752=CARTESIAN_POINT('Ctrl Pts',(-22.4362688521869,26.5743493362595,-1.8250139725686));
#40753=CARTESIAN_POINT('Ctrl Pts',(-22.4344987781511,26.5736967073091,-1.82513111186687));
#40754=CARTESIAN_POINT('Ctrl Pts',(-22.430429216126,26.572192193192,-1.82540029617754));
#40755=CARTESIAN_POINT('Ctrl Pts',(-22.4281301210197,26.5713392354122,-1.82555227643369));
#40756=CARTESIAN_POINT('Ctrl Pts',(-22.4208344318647,26.568623078135,-1.82603425795931));
#40757=CARTESIAN_POINT('Ctrl Pts',(-22.4158414544478,26.5667500882374,-1.82636367307461));
#40758=CARTESIAN_POINT('Ctrl Pts',(-22.3732834351261,26.5506649071019,-1.82916789367756));
#40759=CARTESIAN_POINT('Ctrl Pts',(-22.3359803653261,26.5357632328176,-1.83160207573915));
#40760=CARTESIAN_POINT('Ctrl Pts',(-22.2229924279091,26.4881589839944,-1.83893034184878));
#40761=CARTESIAN_POINT('Ctrl Pts',(-22.1482954939807,26.4532550560576,-1.84371331314543));
#40762=CARTESIAN_POINT('Ctrl Pts',(-22.0750359636318,26.4155367479307,-1.84841977781534));
#40763=CARTESIAN_POINT('Ctrl Pts',(-22.0750363389647,26.4155369411741,-2.09574775951102));
#40764=CARTESIAN_POINT('Ctrl Pts',(-22.2011751392929,26.4804805817286,-2.08670276167943));
#40765=CARTESIAN_POINT('Ctrl Pts',(-22.3315060440038,26.53704528402,-2.07737252921282));
#40766=CARTESIAN_POINT('Ctrl Pts',(-22.7433972891215,26.6843228832894,-2.04808129956067));
#40767=CARTESIAN_POINT('Ctrl Pts',(-23.0339622594772,26.7450714813704,-2.02757079915333));
#40768=CARTESIAN_POINT('Ctrl Pts',(-23.3412669817044,26.7662438687843,-2.00814414337565));
#40769=CARTESIAN_POINT('Ctrl Pts',(-23.3537994529027,26.7670337553,-2.00735601078313));
#40770=CARTESIAN_POINT('Ctrl Pts',(-23.3697931694055,26.7679479754731,-2.00635574359657));
#40771=CARTESIAN_POINT('Ctrl Pts',(-23.3732502102837,26.7681399953631,-2.00613986555109));
#40772=CARTESIAN_POINT('Ctrl Pts',(-23.3787915313267,26.7684388288754,-2.00579436834691));
#40773=CARTESIAN_POINT('Ctrl Pts',(-23.3808756052322,26.7685491890665,-2.00566454930556));
#40774=CARTESIAN_POINT('Ctrl Pts',(-23.3848339188845,26.7687549422693,-2.00541821445588));
#40775=CARTESIAN_POINT('Ctrl Pts',(-23.3867081208446,26.7688507219066,-2.00530167781696));
#40776=CARTESIAN_POINT('Ctrl Pts',(-23.3910005366016,26.7690663235438,-2.005035004047));
#40777=CARTESIAN_POINT('Ctrl Pts',(-23.3934187992127,26.7691850573912,-2.00488492922803));
#40778=CARTESIAN_POINT('Ctrl Pts',(-23.4008658940968,26.7695422889126,-2.00442326890558));
#40779=CARTESIAN_POINT('Ctrl Pts',(-23.4058951840868,26.7697717295606,-2.00411219305613));
#40780=CARTESIAN_POINT('Ctrl Pts',(-23.4438430775558,26.7714138467199,-2.00177014959254));
#40781=CARTESIAN_POINT('Ctrl Pts',(-23.47678259673,26.7723334685427,-1.99976639346848));
#40782=CARTESIAN_POINT('Ctrl Pts',(-23.5180310480813,26.7728521382516,-1.99728726580144));
#40783=CARTESIAN_POINT('Ctrl Pts',(-23.526330592207,26.7729244343096,-1.99678996752611));
#40784=CARTESIAN_POINT('Ctrl Pts',(-23.5407225203228,26.7729941992907,-1.99593012100705));
#40785=CARTESIAN_POINT('Ctrl Pts',(-23.5468147471754,26.7730064565099,-1.99556691725262));
#40786=CARTESIAN_POINT('Ctrl Pts',(-23.8550998779148,26.7727525309378,-1.97722537277802));
#40787=CARTESIAN_POINT('Ctrl Pts',(-24.1557922869066,26.7300028437982,-1.96104434394632));
#40788=CARTESIAN_POINT('Ctrl Pts',(-24.5186042529909,26.6250046732449,-1.93954680566064));
#40789=CARTESIAN_POINT('Ctrl Pts',(-24.5902897000707,26.6015026766257,-1.9352057457857));
#40790=CARTESIAN_POINT('Ctrl Pts',(-24.7352376523306,26.5482799390058,-1.9261689890664));
#40791=CARTESIAN_POINT('Ctrl Pts',(-24.8083620267614,26.5183355824813,-1.92146930241151));
#40792=CARTESIAN_POINT('Ctrl Pts',(-24.8896617974048,26.4814989951999,-1.91605416370084));
#40793=CARTESIAN_POINT('Ctrl Pts',(-24.8989948808137,26.4772163310555,-1.91542964236119));
#40794=CARTESIAN_POINT('Ctrl Pts',(-24.915642800184,26.4694805813602,-1.91431043157827));
#40795=CARTESIAN_POINT('Ctrl Pts',(-24.922965434871,26.4660444095235,-1.91381632819794));
#40796=CARTESIAN_POINT('Ctrl Pts',(-24.9340126918647,26.4608096070354,-1.91306812527711));
#40797=CARTESIAN_POINT('Ctrl Pts',(-24.9377469532686,26.459031295977,-1.91281473200034));
#40798=CARTESIAN_POINT('Ctrl Pts',(-24.9442195520279,26.4559336476926,-1.91237468565196));
#40799=CARTESIAN_POINT('Ctrl Pts',(-24.9469594715196,26.454617613048,-1.91218814778618));
#40800=CARTESIAN_POINT('Ctrl Pts',(-24.9525992394811,26.4518989006218,-1.91180364282047));
#40801=CARTESIAN_POINT('Ctrl Pts',(-24.9554988543054,26.4504957476698,-1.9116056592851));
#40802=CARTESIAN_POINT('Ctrl Pts',(-24.9624758865332,26.4471065715472,-1.91112855889887));
#40803=CARTESIAN_POINT('Ctrl Pts',(-24.966551216833,26.4451162877823,-1.91084929333928));
#40804=CARTESIAN_POINT('Ctrl Pts',(-24.9790502952278,26.4389793564025,-1.90999096721693));
#40805=CARTESIAN_POINT('Ctrl Pts',(-24.9874600779658,26.4348045216594,-1.90941092014022));
#40806=CARTESIAN_POINT('Ctrl Pts',(-25.0184049107969,26.4192737828006,-1.90726710386275));
#40807=CARTESIAN_POINT('Ctrl Pts',(-25.0408241335984,26.4076902980701,-1.90569534638959));
#40808=CARTESIAN_POINT('Ctrl Pts',(-25.068436336152,26.3930103409279,-1.90373591879255));
#40809=CARTESIAN_POINT('Ctrl Pts',(-25.0737601520591,26.3901607266833,-1.90335703126427));
#40810=CARTESIAN_POINT('Ctrl Pts',(-25.0851198953671,26.3840391990825,-1.9025462209027));
#40811=CARTESIAN_POINT('Ctrl Pts',(-25.0911534307059,26.3807629306481,-1.90211414560646));
#40812=CARTESIAN_POINT('Ctrl Pts',(-25.0984883947788,26.3767495706759,-1.90158712523887));
#40813=CARTESIAN_POINT('Ctrl Pts',(-25.0997998745581,26.3760308017155,-1.90149282666959));
#40814=CARTESIAN_POINT('Ctrl Pts',(-25.1036283669803,26.3739290933302,-1.90121734950016));
#40815=CARTESIAN_POINT('Ctrl Pts',(-25.1061440271363,26.3725437046083,-1.9010360847221));
#40816=CARTESIAN_POINT('Ctrl Pts',(-25.1146894318349,26.3678228026043,-1.90041949186207));
#40817=CARTESIAN_POINT('Ctrl Pts',(-25.120710297586,26.3644713310074,-1.89998360349084));
#40818=CARTESIAN_POINT('Ctrl Pts',(-25.1313586658994,26.3584991797639,-1.89921011500283));
#40819=CARTESIAN_POINT('Ctrl Pts',(-25.1359905321879,26.3558862991817,-1.89887278921981));
#40820=CARTESIAN_POINT('Ctrl Pts',(-25.1440995884511,26.3512854063983,-1.89828069805135));
#40821=CARTESIAN_POINT('Ctrl Pts',(-25.1475795885699,26.3493023488016,-1.8980261060129));
#40822=CARTESIAN_POINT('Ctrl Pts',(-25.1548406636712,26.3451467167868,-1.89749385711653));
#40823=CARTESIAN_POINT('Ctrl Pts',(-25.1586210417822,26.3429729463794,-1.89721615906713));
#40824=CARTESIAN_POINT('Ctrl Pts',(-25.1853074313872,26.327555740211,-1.89525165842774));
#40825=CARTESIAN_POINT('Ctrl Pts',(-25.2080534647302,26.3140386375315,-1.89355541964498));
#40826=CARTESIAN_POINT('Ctrl Pts',(-25.3127290524877,26.2500767879286,-1.88564750675736));
#40827=CARTESIAN_POINT('Ctrl Pts',(-25.3925338541213,26.1962629882673,-1.8793234610762));
#40828=CARTESIAN_POINT('Ctrl Pts',(-25.5212403850291,26.1008258788836,-1.86864566928385));
#40829=CARTESIAN_POINT('Ctrl Pts',(-25.5715243284565,26.0611641915785,-1.86434310078712));
#40830=CARTESIAN_POINT('Ctrl Pts',(-25.7109822118129,25.9442609857963,-1.85206195737553));
#40831=CARTESIAN_POINT('Ctrl Pts',(-25.7971445526171,25.863584693704,-1.84404495176569));
#40832=CARTESIAN_POINT('Ctrl Pts',(-25.9431886626645,25.7109647395509,-1.82985284903459));
#40833=CARTESIAN_POINT('Ctrl Pts',(-26.0047346873913,25.64078849053,-1.82365067699451));
#40834=CARTESIAN_POINT('Ctrl Pts',(-26.084091307304,25.5419595864191,-1.81544258652913));
#40835=CARTESIAN_POINT('Ctrl Pts',(-26.1046233779342,25.5155580329806,-1.81329800393248));
#40836=CARTESIAN_POINT('Ctrl Pts',(-26.1354081421401,25.4746751628591,-1.81005594771835));
#40837=CARTESIAN_POINT('Ctrl Pts',(-26.1459578348705,25.4604216359595,-1.80893994149941));
#40838=CARTESIAN_POINT('Ctrl Pts',(-26.1586761428049,25.442938172625,-1.80758912512211));
#40839=CARTESIAN_POINT('Ctrl Pts',(-26.1609569854512,25.4397908154816,-1.80734666072015));
#40840=CARTESIAN_POINT('Ctrl Pts',(-26.1645090066659,25.4348706373559,-1.80696873717648));
#40841=CARTESIAN_POINT('Ctrl Pts',(-26.1657840790539,25.4331006524819,-1.80683300750787));
#40842=CARTESIAN_POINT('Ctrl Pts',(-26.1680363061781,25.4299675328271,-1.80659314601665));
#40843=CARTESIAN_POINT('Ctrl Pts',(-26.1690141887757,25.4286049370917,-1.80648896346828));
#40844=CARTESIAN_POINT('Ctrl Pts',(-26.1711029408282,25.4256896381597,-1.80626634776544));
#40845=CARTESIAN_POINT('Ctrl Pts',(-26.1722134911821,25.4241367155044,-1.8061479370324));
#40846=CARTESIAN_POINT('Ctrl Pts',(-26.1754223003678,25.4196412845054,-1.80580565454605));
#40847=CARTESIAN_POINT('Ctrl Pts',(-26.1775169989933,25.4166962202813,-1.80558203013265));
#40848=CARTESIAN_POINT('Ctrl Pts',(-26.1868323180954,25.4035524917458,-1.80458670053755));
#40849=CARTESIAN_POINT('Ctrl Pts',(-26.1939986666674,25.3933152267318,-1.80381869765335));
#40850=CARTESIAN_POINT('Ctrl Pts',(-26.3152436862393,25.2179520936328,-1.79078095830451));
#40851=CARTESIAN_POINT('Ctrl Pts',(-26.4137310232875,25.0425377726757,-1.77950292950655));
#40852=CARTESIAN_POINT('Ctrl Pts',(-26.5612345127091,24.710636417083,-1.7591881289436));
#40853=CARTESIAN_POINT('Ctrl Pts',(-26.6158846970046,24.5574266515223,-1.75016279157195));
#40854=CARTESIAN_POINT('Ctrl Pts',(-26.6915335483904,24.2809387701899,-1.73371922736902));
#40855=CARTESIAN_POINT('Ctrl Pts',(-26.7173582157115,24.159337857078,-1.72643949757995));
#40856=CARTESIAN_POINT('Ctrl Pts',(-26.7391736186868,24.0164228794936,-1.71769444918471));
#40857=CARTESIAN_POINT('Ctrl Pts',(-26.7420563474737,23.9962579847636,-1.71645637202738));
#40858=CARTESIAN_POINT('Ctrl Pts',(-26.7455395984723,23.9701263783485,-1.71484613823199));
#40859=CARTESIAN_POINT('Ctrl Pts',(-26.7463149455236,23.964183120518,-1.71447952559014));
#40860=CARTESIAN_POINT('Ctrl Pts',(-26.7475420487022,23.954567994543,-1.71388577271022));
#40861=CARTESIAN_POINT('Ctrl Pts',(-26.7480040719188,23.9508974316715,-1.71365895770139));
#40862=CARTESIAN_POINT('Ctrl Pts',(-26.7488748480599,23.9438820461965,-1.7132251653749));
#40863=CARTESIAN_POINT('Ctrl Pts',(-26.7492846775162,23.940537360121,-1.71301822241602));
#40864=CARTESIAN_POINT('Ctrl Pts',(-26.7502108949041,23.9328788662033,-1.71254408319146));
#40865=CARTESIAN_POINT('Ctrl Pts',(-26.7507238060361,23.92856465145,-1.71227677736607));
#40866=CARTESIAN_POINT('Ctrl Pts',(-26.7522743046873,23.9152941987828,-1.71145389050412));
#40867=CARTESIAN_POINT('Ctrl Pts',(-26.7532830259138,23.9063346905873,-1.71089739854318));
#40868=CARTESIAN_POINT('Ctrl Pts',(-26.7605977734794,23.8388175297896,-1.70669668215556));
#40869=CARTESIAN_POINT('Ctrl Pts',(-26.7653347541892,23.7801044212592,-1.70300322056571));
#40870=CARTESIAN_POINT('Ctrl Pts',(-26.7692479267539,23.7064781441524,-1.69831664865356));
#40871=CARTESIAN_POINT('Ctrl Pts',(-26.7699331803443,23.6916537499286,-1.69737025914913));
#40872=CARTESIAN_POINT('Ctrl Pts',(-26.7722017411626,23.6339370617008,-1.69367479996766));
#40873=CARTESIAN_POINT('Ctrl Pts',(-26.7730304438053,23.5910210324962,-1.69090365196987));
#40874=CARTESIAN_POINT('Ctrl Pts',(-26.7729009589345,23.3969072731341,-1.6782653603257));
#40875=CARTESIAN_POINT('Ctrl Pts',(-26.762160312742,23.245921019536,-1.6681369661269));
#40876=CARTESIAN_POINT('Ctrl Pts',(-26.708051016869,22.8656459064639,-1.64217120326962));
#40877=CARTESIAN_POINT('Ctrl Pts',(-26.6503278496435,22.6392464702608,-1.62625582676243));
#40878=CARTESIAN_POINT('Ctrl Pts',(-26.5637957857494,22.4079434969898,-1.61065726557838));
#40879=CARTESIAN_POINT('Ctrl Pts',(-26.5588137394052,22.3948857712107,-1.60977919307569));
#40880=CARTESIAN_POINT('Ctrl Pts',(-26.5523956841853,22.3783873759847,-1.60867331656203));
#40881=CARTESIAN_POINT('Ctrl Pts',(-26.5510385354166,22.3749164897838,-1.60844086601903));
#40882=CARTESIAN_POINT('Ctrl Pts',(-26.548882312421,22.369430063493,-1.60807375827423));
#40883=CARTESIAN_POINT('Ctrl Pts',(-26.5480872250465,22.3674129759342,-1.60793886084429));
#40884=CARTESIAN_POINT('Ctrl Pts',(-26.5466043480409,22.3636621077525,-1.6076881450184));
#40885=CARTESIAN_POINT('Ctrl Pts',(-26.54591709312,22.3619281328188,-1.60757229538596));
#40886=CARTESIAN_POINT('Ctrl Pts',(-26.5443797753195,22.3580592202002,-1.6073139244837));
#40887=CARTESIAN_POINT('Ctrl Pts',(-26.5435289361523,22.355924599515,-1.60717145135671));
#40888=CARTESIAN_POINT('Ctrl Pts',(-26.5410316618907,22.3496787648553,-1.60675480721923));
#40889=CARTESIAN_POINT('Ctrl Pts',(-26.5393790262915,22.3455700112375,-1.60648101169907));
#40890=CARTESIAN_POINT('Ctrl Pts',(-26.5272172931887,22.3155128298761,-1.6044801154671));
#40891=CARTESIAN_POINT('Ctrl Pts',(-26.5163785243098,22.2896978732313,-1.60277269959519));
#40892=CARTESIAN_POINT('Ctrl Pts',(-26.4799458170619,22.2059980564678,-1.5972627553313));
#40893=CARTESIAN_POINT('Ctrl Pts',(-26.4529817048122,22.14872218552,-1.59353320328476));
#40894=CARTESIAN_POINT('Ctrl Pts',(-26.3861173932511,22.0169134675127,-1.58496314952343));
#40895=CARTESIAN_POINT('Ctrl Pts',(-26.3449371428071,21.9430818542706,-1.58017215715433));
#40896=CARTESIAN_POINT('Ctrl Pts',(-26.1671499737347,21.6518715629132,-1.56098845376566));
#40897=CARTESIAN_POINT('Ctrl Pts',(-26.0077178421121,21.4495715898968,-1.54690720546562));
#40898=CARTESIAN_POINT('Ctrl Pts',(-25.8171539791868,21.2595254115901,-1.53111138195038));
#40899=CARTESIAN_POINT('Ctrl Pts',(-25.8082777887953,21.2507754511653,-1.53037790260144));
#40900=CARTESIAN_POINT('Ctrl Pts',(-25.7505495017093,21.1945246918028,-1.52562138434387));
#40901=CARTESIAN_POINT('Ctrl Pts',(-25.7002550866962,21.1485347340481,-1.52154038953863));
#40902=CARTESIAN_POINT('Ctrl Pts',(-25.6414048432671,21.0980518802236,-1.51681763112022));
#40903=CARTESIAN_POINT('Ctrl Pts',(-25.6342393539314,21.0919594354463,-1.51624346249569));
#40904=CARTESIAN_POINT('Ctrl Pts',(-25.6237035441359,21.0830805507818,-1.51540045047024));
#40905=CARTESIAN_POINT('Ctrl Pts',(-25.6203540126742,21.0802694259746,-1.51513262045078));
#40906=CARTESIAN_POINT('Ctrl Pts',(-25.6144021684953,21.0752948973606,-1.51465702095385));
#40907=CARTESIAN_POINT('Ctrl Pts',(-25.6118021449282,21.0731287546318,-1.5144493638413));
#40908=CARTESIAN_POINT('Ctrl Pts',(-25.6063898249814,21.0686340426976,-1.51401731212067));
#40909=CARTESIAN_POINT('Ctrl Pts',(-25.603576974891,21.0663061505153,-1.5137928903504));
#40910=CARTESIAN_POINT('Ctrl Pts',(-25.5963032366952,21.0603072610351,-1.51321286680965));
#40911=CARTESIAN_POINT('Ctrl Pts',(-25.5918364368312,21.0566434813612,-1.51285697260819));
#40912=CARTESIAN_POINT('Ctrl Pts',(-25.573071297979,21.0413360686713,-1.5113630748757));
#40913=CARTESIAN_POINT('Ctrl Pts',(-25.5586832366834,21.0298034327893,-1.51022060000891));
#40914=CARTESIAN_POINT('Ctrl Pts',(-25.4610349155357,20.9529012542054,-1.5024856489804));
#40915=CARTESIAN_POINT('Ctrl Pts',(-25.3747051737642,20.8915514704308,-1.49573507548004));
#40916=CARTESIAN_POINT('Ctrl Pts',(-25.1572168827541,20.752580899112,-1.47891845934216));
#40917=CARTESIAN_POINT('Ctrl Pts',(-25.0232759441968,20.6798005496214,-1.46871095979811));
#40918=CARTESIAN_POINT('Ctrl Pts',(-24.6745928147253,20.5211833562646,-1.44280913980538));
#40919=CARTESIAN_POINT('Ctrl Pts',(-24.4547972687646,20.44844309298,-1.42705018909865));
#40920=CARTESIAN_POINT('Ctrl Pts',(-24.2161974415993,20.3970305152307,-1.41164456000963));
#40921=CARTESIAN_POINT('Ctrl Pts',(-24.2032798816226,20.3943300037023,-1.41081579340468));
#40922=CARTESIAN_POINT('Ctrl Pts',(-24.1867715361973,20.3909845120886,-1.40976369733969));
#40923=CARTESIAN_POINT('Ctrl Pts',(-24.1831959887697,20.3902662274114,-1.40953624476675));
#40924=CARTESIAN_POINT('Ctrl Pts',(-24.1775110747314,20.3891342322424,-1.40917528603247));
#40925=CARTESIAN_POINT('Ctrl Pts',(-24.1754025138489,20.3887165627672,-1.40904155284713));
#40926=CARTESIAN_POINT('Ctrl Pts',(-24.1714980719402,20.3879472191013,-1.40879419396643));
#40927=CARTESIAN_POINT('Ctrl Pts',(-24.1697023210212,20.3875949672623,-1.4086805356983));
#40928=CARTESIAN_POINT('Ctrl Pts',(-24.1657777946103,20.3868286087409,-1.40843237693538));
#40929=CARTESIAN_POINT('Ctrl Pts',(-24.1636489062009,20.386415122248,-1.40829791273573));
#40930=CARTESIAN_POINT('Ctrl Pts',(-24.159156195249,20.3855472239108,-1.40801446169817));
#40931=CARTESIAN_POINT('Ctrl Pts',(-24.1567922762052,20.3850933105776,-1.4078655035266));
#40932=CARTESIAN_POINT('Ctrl Pts',(-24.1506977816074,20.3839301405734,-1.40748194025754));
#40933=CARTESIAN_POINT('Ctrl Pts',(-24.1469664436035,20.3832248257312,-1.40724755886948));
#40934=CARTESIAN_POINT('Ctrl Pts',(-24.1360862728115,20.3811881164023,-1.40656542907959));
#40935=CARTESIAN_POINT('Ctrl Pts',(-24.1289341124098,20.3798743096192,-1.4061186615157));
#40936=CARTESIAN_POINT('Ctrl Pts',(-24.0547172706226,20.3665006590652,-1.40149900089485));
#40937=CARTESIAN_POINT('Ctrl Pts',(-23.9872849340557,20.3565454536014,-1.39744013883199));
#40938=CARTESIAN_POINT('Ctrl Pts',(-23.8513455204538,20.3408633707872,-1.38944356119344));
#40939=CARTESIAN_POINT('Ctrl Pts',(-23.7828709959598,20.3351747117281,-1.38550909849417));
#40940=CARTESIAN_POINT('Ctrl Pts',(-23.362455779992,20.3137513059831,-1.36165200210973));
#40941=CARTESIAN_POINT('Ctrl Pts',(-23.0101247566829,20.3536182663799,-1.34262619544138));
#40942=CARTESIAN_POINT('Ctrl Pts',(-22.6512580904904,20.4553604653162,-1.32007313505219));
#40943=CARTESIAN_POINT('Ctrl Pts',(-22.6313553927862,20.4612112686684,-1.31881273758147));
#40944=CARTESIAN_POINT('Ctrl Pts',(-22.6054875482102,20.4690877627669,-1.3171615742955));
#40945=CARTESIAN_POINT('Ctrl Pts',(-22.5994695960322,20.4709394564027,-1.31677652258074));
#40946=CARTESIAN_POINT('Ctrl Pts',(-22.5902194017627,20.4738153962714,-1.31618322754854));
#40947=CARTESIAN_POINT('Ctrl Pts',(-22.5869832615334,20.4748271348103,-1.31597539570229));
#40948=CARTESIAN_POINT('Ctrl Pts',(-22.5805905616292,20.4768368119964,-1.31556430612857));
#40949=CARTESIAN_POINT('Ctrl Pts',(-22.5774339306523,20.4778345113701,-1.31536105649232));
#40950=CARTESIAN_POINT('Ctrl Pts',(-22.5704416515864,20.4800563795656,-1.31491025970654));
#40951=CARTESIAN_POINT('Ctrl Pts',(-22.5666067535526,20.4812828745891,-1.31466263613482));
#40952=CARTESIAN_POINT('Ctrl Pts',(-22.5556611527179,20.484806171233,-1.3139547602697));
#40953=CARTESIAN_POINT('Ctrl Pts',(-22.5485561609215,20.4871205104988,-1.31349392966345));
#40954=CARTESIAN_POINT('Ctrl Pts',(-22.5033881026817,20.5020072506236,-1.3105557402038));
#40955=CARTESIAN_POINT('Ctrl Pts',(-22.4655557668092,20.5152637145138,-1.30805581643115));
#40956=CARTESIAN_POINT('Ctrl Pts',(-22.3538663948609,20.556754755859,-1.30055505315203));
#40957=CARTESIAN_POINT('Ctrl Pts',(-22.2807948901364,20.5870035900472,-1.29548825641569));
#40958=CARTESIAN_POINT('Ctrl Pts',(-22.0714517310497,20.682828450085,-1.28049853754635));
#40959=CARTESIAN_POINT('Ctrl Pts',(-21.9386005323521,20.7553389150149,-1.2703713642156));
#40960=CARTESIAN_POINT('Ctrl Pts',(-21.6314521642055,20.9521814800467,-1.24571000850892));
#40961=CARTESIAN_POINT('Ctrl Pts',(-21.463460463427,21.0850787648623,-1.23112807469708));
#40962=CARTESIAN_POINT('Ctrl Pts',(-21.3066056699675,21.2367731837902,-1.2171557165846));
#40963=CARTESIAN_POINT('Ctrl Pts',(-21.3033678639448,21.2399176590724,-1.21686714446093));
#40964=CARTESIAN_POINT('Ctrl Pts',(-21.2963793619282,21.246733301936,-1.2162439760432));
#40965=CARTESIAN_POINT('Ctrl Pts',(-21.2926309974804,21.250406859404,-1.21590953668217));
#40966=CARTESIAN_POINT('Ctrl Pts',(-21.282618080161,21.2602680149908,-1.21501567259362));
#40967=CARTESIAN_POINT('Ctrl Pts',(-21.2763698307259,21.2664722097875,-1.21445737438463));
#40968=CARTESIAN_POINT('Ctrl Pts',(-21.2598448061077,21.2830157725445,-1.21297965249756));
#40969=CARTESIAN_POINT('Ctrl Pts',(-21.249612468608,21.2933995478286,-1.21206343507456));
#40970=CARTESIAN_POINT('Ctrl Pts',(-21.2368116679226,21.3065673339627,-1.21091612530259));
#40971=CARTESIAN_POINT('Ctrl Pts',(-21.2341773913626,21.3092867038921,-1.21067996069684));
#40972=CARTESIAN_POINT('Ctrl Pts',(-21.2300325397459,21.3135805592881,-1.21030828707244));
#40973=CARTESIAN_POINT('Ctrl Pts',(-21.2285187717058,21.315151936423,-1.21017252780909));
#40974=CARTESIAN_POINT('Ctrl Pts',(-21.225739944152,21.3180423863112,-1.20992328330767));
#40975=CARTESIAN_POINT('Ctrl Pts',(-21.2244744182807,21.3193609901816,-1.20980976147508));
#40976=CARTESIAN_POINT('Ctrl Pts',(-21.2216748958573,21.3222828999342,-1.209558608897));
#40977=CARTESIAN_POINT('Ctrl Pts',(-21.220141436946,21.3238867099194,-1.20942102051637));
#40978=CARTESIAN_POINT('Ctrl Pts',(-21.2169589162153,21.3272221260803,-1.2091354312578));
#40979=CARTESIAN_POINT('Ctrl Pts',(-21.2153101218947,21.3289539873003,-1.20898745126677));
#40980=CARTESIAN_POINT('Ctrl Pts',(-21.2110740128681,21.3334134411331,-1.20860719580412));
#40981=CARTESIAN_POINT('Ctrl Pts',(-21.2084895316137,21.3361437384847,-1.20837513865686));
#40982=CARTESIAN_POINT('Ctrl Pts',(-21.2009886047108,21.3440956921651,-1.20770144187643));
#40983=CARTESIAN_POINT('Ctrl Pts',(-21.1960847656151,21.3493292866326,-1.20726075400568));
#40984=CARTESIAN_POINT('Ctrl Pts',(-21.0696286689402,21.4851950294501,-1.19588882381541));
#40985=CARTESIAN_POINT('Ctrl Pts',(-20.9590965341054,21.6257037763544,-1.18575284308195));
#40986=CARTESIAN_POINT('Ctrl Pts',(-20.6882115155567,22.0360150351246,-1.15816782537698));
#40987=CARTESIAN_POINT('Ctrl Pts',(-20.5547041435692,22.321080676087,-1.14094732402074));
#40988=CARTESIAN_POINT('Ctrl Pts',(-20.458998071584,22.638871702962,-1.12085696781627));
#40989=CARTESIAN_POINT('Ctrl Pts',(-20.4537478671096,22.6568724383445,-1.11971691007044));
#40990=CARTESIAN_POINT('Ctrl Pts',(-20.447011973554,22.6807399100413,-1.11820222218321));
#40991=CARTESIAN_POINT('Ctrl Pts',(-20.4453852243013,22.6865667302628,-1.11783219752102));
#40992=CARTESIAN_POINT('Ctrl Pts',(-20.442885600431,22.6956184120386,-1.1172569975411));
#40993=CARTESIAN_POINT('Ctrl Pts',(-20.4420013117371,22.698840130159,-1.11705219408571));
#40994=CARTESIAN_POINT('Ctrl Pts',(-20.4402411246179,22.705292288061,-1.11664187921063));
#40995=CARTESIAN_POINT('Ctrl Pts',(-20.4393652459643,22.708522728957,-1.11643636743425));
#40996=CARTESIAN_POINT('Ctrl Pts',(-20.4374213860382,22.7157366064281,-1.11597726603841));
#40997=CARTESIAN_POINT('Ctrl Pts',(-20.436356016792,22.7197207351227,-1.11572359191395));
#40998=CARTESIAN_POINT('Ctrl Pts',(-20.4332637107434,22.731374528016,-1.11498122876439));
#40999=CARTESIAN_POINT('Ctrl Pts',(-20.4312574527445,22.7390496036151,-1.11449186950533));
#41000=CARTESIAN_POINT('Ctrl Pts',(-20.416797891624,22.7952123212608,-1.11090759921212));
#41001=CARTESIAN_POINT('Ctrl Pts',(-20.4054481360072,22.8439745709118,-1.10777716520858));
#41002=CARTESIAN_POINT('Ctrl Pts',(-20.3721754995751,23.0036883718675,-1.09745623167664));
#41003=CARTESIAN_POINT('Ctrl Pts',(-20.354957351514,23.1155228636957,-1.09012041782651));
#41004=CARTESIAN_POINT('Ctrl Pts',(-20.309810320198,23.5647912239797,-1.06026011071333));
#41005=CARTESIAN_POINT('Ctrl Pts',(-20.3292301653878,23.9047540870365,-1.03654077099051));
#41006=CARTESIAN_POINT('Ctrl Pts',(-20.4020321778134,24.2393403342527,-1.01489042254365));
#41007=CARTESIAN_POINT('Ctrl Pts',(-20.402885405708,24.2432269690667,-1.01463920028158));
#41008=CARTESIAN_POINT('Ctrl Pts',(-20.4063010843938,24.2586496701697,-1.01364342873332));
#41009=CARTESIAN_POINT('Ctrl Pts',(-20.4089198213766,24.2701733760852,-1.01290187038063));
#41010=CARTESIAN_POINT('Ctrl Pts',(-20.4124045846724,24.2851268958564,-1.0119430522834));
#41011=CARTESIAN_POINT('Ctrl Pts',(-20.4132129092912,24.2885698601455,-1.01172252797463));
#41012=CARTESIAN_POINT('Ctrl Pts',(-20.4144627339557,24.2938542345521,-1.01138443336166));
#41013=CARTESIAN_POINT('Ctrl Pts',(-20.4149001888925,24.2956965836696,-1.01126662947618));
#41014=CARTESIAN_POINT('Ctrl Pts',(-20.4157299907772,24.2991776563292,-1.01104417519294));
#41015=CARTESIAN_POINT('Ctrl Pts',(-20.4161219973826,24.3008164501932,-1.0109395057837));
#41016=CARTESIAN_POINT('Ctrl Pts',(-20.4170196724174,24.3045562383449,-1.01070077387203));
#41017=CARTESIAN_POINT('Ctrl Pts',(-20.4175261678783,24.306657027872,-1.01056676023376));
#41018=CARTESIAN_POINT('Ctrl Pts',(-20.4189414775473,24.3125014973824,-1.01019418078611));
#41019=CARTESIAN_POINT('Ctrl Pts',(-20.4198548957881,24.316244075379,-1.00995588185317));
#41020=CARTESIAN_POINT('Ctrl Pts',(-20.4219089221042,24.3245950663587,-1.00942477655976));
#41021=CARTESIAN_POINT('Ctrl Pts',(-20.4230530095223,24.3292026262787,-1.00913216910047));
#41022=CARTESIAN_POINT('Ctrl Pts',(-20.4266068317581,24.3433808359462,-1.00823302583629));
#41023=CARTESIAN_POINT('Ctrl Pts',(-20.4290503790251,24.3529430659052,-1.00762838123761));
#41024=CARTESIAN_POINT('Ctrl Pts',(-20.4382519380361,24.3882737355535,-1.00540035910864));
#41025=CARTESIAN_POINT('Ctrl Pts',(-20.4452856579359,24.4139701062999,-1.00379177954574));
#41026=CARTESIAN_POINT('Ctrl Pts',(-20.4765220965681,24.5227700353375,-0.997020079348007));
#41027=CARTESIAN_POINT('Ctrl Pts',(-20.5037505359669,24.604973873176,-0.992000840985586));
#41028=CARTESIAN_POINT('Ctrl Pts',(-20.6402645512784,24.9674928058054,-0.969900176978225));
#41029=CARTESIAN_POINT('Ctrl Pts',(-20.7851540369272,25.2327630591764,-0.953670432714227));
#41030=CARTESIAN_POINT('Ctrl Pts',(-20.977078177054,25.4906955230521,-0.934840809804062));
#41031=CARTESIAN_POINT('Ctrl Pts',(-20.9895830599513,25.5071677296483,-0.933624294109055));
#41032=CARTESIAN_POINT('Ctrl Pts',(-21.0052465112645,25.5273933820429,-0.932112465217948));
#41033=CARTESIAN_POINT('Ctrl Pts',(-21.0082564217634,25.5312617095809,-0.931822486799601));
#41034=CARTESIAN_POINT('Ctrl Pts',(-21.0137535321157,25.5382934218109,-0.931293850958268));
#41035=CARTESIAN_POINT('Ctrl Pts',(-21.0162378581375,25.5414590477622,-0.93105529814438));
#41036=CARTESIAN_POINT('Ctrl Pts',(-21.0214071166785,25.5480205789189,-0.930559657802778));
#41037=CARTESIAN_POINT('Ctrl Pts',(-21.0240929744663,25.5514157421107,-0.930302536624922));
#41038=CARTESIAN_POINT('Ctrl Pts',(-21.0595499577223,25.5960513917799,-0.926913448913421));
#41039=CARTESIAN_POINT('Ctrl Pts',(-21.0933189959918,25.6364858348869,-0.923744519564235));
#41040=CARTESIAN_POINT('Ctrl Pts',(-21.1338138871127,25.6826262952294,-0.920003305402341));
#41041=CARTESIAN_POINT('Ctrl Pts',(-21.1395919864224,25.6891562984767,-0.919470833231494));
#41042=CARTESIAN_POINT('Ctrl Pts',(-21.1482494170282,25.6988606778806,-0.918674991332547));
#41043=CARTESIAN_POINT('Ctrl Pts',(-21.1511087288068,25.7020529270631,-0.91841246437401));
#41044=CARTESIAN_POINT('Ctrl Pts',(-21.1562227678772,25.7077395787713,-0.917943481413285));
#41045=CARTESIAN_POINT('Ctrl Pts',(-21.1584750516817,25.7102361784646,-0.917737128877092));
#41046=CARTESIAN_POINT('Ctrl Pts',(-21.1632346883992,25.7154955430007,-0.917301458772015));
#41047=CARTESIAN_POINT('Ctrl Pts',(-21.1657429384674,25.7182574859881,-0.917072103306014));
#41048=CARTESIAN_POINT('Ctrl Pts',(-21.1723875224505,25.7255486456641,-0.916465136922146));
#41049=CARTESIAN_POINT('Ctrl Pts',(-21.1765319857922,25.7300704036202,-0.916087180152197));
#41050=CARTESIAN_POINT('Ctrl Pts',(-21.1954078558245,25.750546986173,-0.914368603810139));
#41051=CARTESIAN_POINT('Ctrl Pts',(-21.2102871076739,25.7663641965461,-0.913021659075345));
#41052=CARTESIAN_POINT('Ctrl Pts',(-21.3209819512588,25.8816792635215,-0.903055598655631));
#41053=CARTESIAN_POINT('Ctrl Pts',(-21.4229334448893,25.9750622798637,-0.894164171201551));
#41054=CARTESIAN_POINT('Ctrl Pts',(-21.6422388991004,26.1514339748723,-0.875591668495027));
#41055=CARTESIAN_POINT('Ctrl Pts',(-21.7597903274098,26.2337019197543,-0.865913501870995));
#41056=CARTESIAN_POINT('Ctrl Pts',(-21.9454058127333,26.3459641497493,-0.851229451117898));
#41057=CARTESIAN_POINT('Ctrl Pts',(-22.0096510653896,26.3818727729581,-0.846249054954694));
#41058=CARTESIAN_POINT('Ctrl Pts',(-22.0750363147453,26.4155369287046,-0.841310143832837));
#41059=CARTESIAN_POINT('Origin',(-23.5502525316942,23.5502525316942,-77.3107734492734));
#41060=CARTESIAN_POINT('',(-22.0750360011372,26.4155367672407,0.656690934610686));
#41061=CARTESIAN_POINT('',(-22.0750360367128,26.4155367855571,0.408876748608879));
#41062=CARTESIAN_POINT('',(-22.0750360153461,26.4155367745563,-77.3107734492734));
#41063=CARTESIAN_POINT('Ctrl Pts',(-22.0750360011372,26.4155367672407,0.656690934610686));
#41064=CARTESIAN_POINT('Ctrl Pts',(-22.0347854868283,26.3948134395739,0.653836575818294));
#41065=CARTESIAN_POINT('Ctrl Pts',(-21.9949738925344,26.3732431361297,0.650952707466448));
#41066=CARTESIAN_POINT('Ctrl Pts',(-21.6767862317566,26.1920704356087,0.627403182791127));
#41067=CARTESIAN_POINT('Ctrl Pts',(-21.4232414642238,25.9925525060078,0.605233911009184));
#41068=CARTESIAN_POINT('Ctrl Pts',(-21.1381756976759,25.6896594749138,0.577578533526645));
#41069=CARTESIAN_POINT('Ctrl Pts',(-21.0760394129289,25.6174849869373,0.571357342939539));
#41070=CARTESIAN_POINT('Ctrl Pts',(-21.0117377680158,25.5357343265099,0.564793087957518));
#41071=CARTESIAN_POINT('Ctrl Pts',(-21.006320034543,25.5287880044894,0.564238981182645));
#41072=CARTESIAN_POINT('Ctrl Pts',(-20.997019697702,25.5167622646266,0.563286106674382));
#41073=CARTESIAN_POINT('Ctrl Pts',(-20.993123634078,25.5116933890586,0.562886419979856));
#41074=CARTESIAN_POINT('Ctrl Pts',(-20.9876218770747,25.504491211832,0.562321321426151));
#41075=CARTESIAN_POINT('Ctrl Pts',(-20.986003744071,25.5023674991691,0.562155034155368));
#41076=CARTESIAN_POINT('Ctrl Pts',(-20.9832287146955,25.4987160181079,0.561869715919636));
#41077=CARTESIAN_POINT('Ctrl Pts',(-20.9820705403344,25.4971892266721,0.561750593893924));
#41078=CARTESIAN_POINT('Ctrl Pts',(-20.9798564189393,25.4942649940674,0.561522783573879));
#41079=CARTESIAN_POINT('Ctrl Pts',(-20.9788002507879,25.4928677270909,0.561414079360236));
#41080=CARTESIAN_POINT('Ctrl Pts',(-20.9763185820844,25.4895790114672,0.561158572940399));
#41081=CARTESIAN_POINT('Ctrl Pts',(-20.9748940241208,25.4876868479115,0.561011837768286));
#41082=CARTESIAN_POINT('Ctrl Pts',(-20.9707034589361,25.4821079575446,0.560579991721011));
#41083=CARTESIAN_POINT('Ctrl Pts',(-20.9679432581271,25.4784168456022,0.560295288733591));
#41084=CARTESIAN_POINT('Ctrl Pts',(-20.9443789238096,25.4467637974791,0.55786238455405));
#41085=CARTESIAN_POINT('Ctrl Pts',(-20.9240207052318,25.4184706337941,0.555744800891914));
#41086=CARTESIAN_POINT('Ctrl Pts',(-20.7258279934546,25.1333849524081,0.534908955592302));
#41087=CARTESIAN_POINT('Ctrl Pts',(-20.5857363473156,24.8523240114919,0.518227634219056));
#41088=CARTESIAN_POINT('Ctrl Pts',(-20.4644387260804,24.4828363782198,0.496108203453257));
#41089=CARTESIAN_POINT('Ctrl Pts',(-20.4431909785306,24.4093956615494,0.491711965062886));
#41090=CARTESIAN_POINT('Ctrl Pts',(-20.4050726640934,24.2576216716744,0.482558403129002));
#41091=CARTESIAN_POINT('Ctrl Pts',(-20.3884723181591,24.1792769723601,0.477797032890339));
#41092=CARTESIAN_POINT('Ctrl Pts',(-20.37216193219,24.0851336079763,0.472000729462033));
#41093=CARTESIAN_POINT('Ctrl Pts',(-20.3696271677712,24.0698484378397,0.471057345330194));
#41094=CARTESIAN_POINT('Ctrl Pts',(-20.3663569315904,24.0492070265632,0.46978010480062));
#41095=CARTESIAN_POINT('Ctrl Pts',(-20.3655245439493,24.0438661698986,0.469449330506847));
#41096=CARTESIAN_POINT('Ctrl Pts',(-20.3642308279089,24.0354257845988,0.468926119387076));
#41097=CARTESIAN_POINT('Ctrl Pts',(-20.3637605743487,24.0323276171166,0.468733966191606));
#41098=CARTESIAN_POINT('Ctrl Pts',(-20.3628136774373,24.0260272620999,0.468343001264512));
#41099=CARTESIAN_POINT('Ctrl Pts',(-20.3623373391534,24.0228250327639,0.468144180079909));
#41100=CARTESIAN_POINT('Ctrl Pts',(-20.3612577706451,24.0154916176718,0.467688609121825));
#41101=CARTESIAN_POINT('Ctrl Pts',(-20.3606577423294,24.0113599730948,0.467431758111159));
#41102=CARTESIAN_POINT('Ctrl Pts',(-20.35890974435,23.9991570205741,0.466672594943795));
#41103=CARTESIAN_POINT('Ctrl Pts',(-20.357784377465,23.9910825542019,0.466169567132753));
#41104=CARTESIAN_POINT('Ctrl Pts',(-20.3505989355672,23.9380563624841,0.46286139372817));
#41105=CARTESIAN_POINT('Ctrl Pts',(-20.3454580638468,23.892987160979,0.460027294462243));
#41106=CARTESIAN_POINT('Ctrl Pts',(-20.3411450070381,23.8464759217142,0.457077673210773));
#41107=CARTESIAN_POINT('Ctrl Pts',(-20.3410206404389,23.8451255039042,0.45699201182157));
#41108=CARTESIAN_POINT('Ctrl Pts',(-20.3369257736191,23.8003525003089,0.454151203607914));
#41109=CARTESIAN_POINT('Ctrl Pts',(-20.3338362481713,23.7568556438337,0.451369095263529));
#41110=CARTESIAN_POINT('Ctrl Pts',(-20.3201322647396,23.486351967586,0.433926681970065));
#41111=CARTESIAN_POINT('Ctrl Pts',(-20.3326739904699,23.2588428614664,0.418576055951041));
#41112=CARTESIAN_POINT('Ctrl Pts',(-20.3982213584296,22.8544729304243,0.390857485635323));
#41113=CARTESIAN_POINT('Ctrl Pts',(-20.4426638453245,22.6771439027861,0.378567211908465));
#41114=CARTESIAN_POINT('Ctrl Pts',(-20.5070500331622,22.489455892002,0.36601620347792));
#41115=CARTESIAN_POINT('Ctrl Pts',(-20.5123269575011,22.4744369394828,0.365015281847339));
#41116=CARTESIAN_POINT('Ctrl Pts',(-20.5189857913965,22.4559246070893,0.36378632773665));
#41117=CARTESIAN_POINT('Ctrl Pts',(-20.5202626848979,22.4523940772207,0.363552166763792));
#41118=CARTESIAN_POINT('Ctrl Pts',(-20.5222812318347,22.4468432689323,0.363184360351415));
#41119=CARTESIAN_POINT('Ctrl Pts',(-20.5230187392951,22.444821502573,0.363050467400887));
#41120=CARTESIAN_POINT('Ctrl Pts',(-20.5243996492584,22.4410476903996,0.362800682117746));
#41121=CARTESIAN_POINT('Ctrl Pts',(-20.525042544358,22.4392954764281,0.362684760546014));
#41122=CARTESIAN_POINT('Ctrl Pts',(-20.526487509072,22.4353677724193,0.36242503924669));
#41123=CARTESIAN_POINT('Ctrl Pts',(-20.5272904026795,22.4331925936731,0.362281290060201));
#41124=CARTESIAN_POINT('Ctrl Pts',(-20.5293337788934,22.4276750682295,0.361916870660934));
#41125=CARTESIAN_POINT('Ctrl Pts',(-20.5305774650981,22.4243339001047,0.361696392631806));
#41126=CARTESIAN_POINT('Ctrl Pts',(-20.5374150247963,22.406057588195,0.36049141931253));
#41127=CARTESIAN_POINT('Ctrl Pts',(-20.5431142873678,22.3911617173432,0.359513161126289));
#41128=CARTESIAN_POINT('Ctrl Pts',(-20.6549957199676,22.1051234590149,0.340791038152935));
#41129=CARTESIAN_POINT('Ctrl Pts',(-20.7973513980028,21.8495146838571,0.325066312705371));
#41130=CARTESIAN_POINT('Ctrl Pts',(-21.0922266244122,21.4563860081436,0.297407822078719));
#41131=CARTESIAN_POINT('Ctrl Pts',(-21.2269414663724,21.3078484597269,0.285904464831211));
#41132=CARTESIAN_POINT('Ctrl Pts',(-21.3850562812297,21.1631526687265,0.272892029846063));
#41133=CARTESIAN_POINT('Ctrl Pts',(-21.3956305867839,21.1536038667641,0.272024105532997));
#41134=CARTESIAN_POINT('Ctrl Pts',(-21.4101727703592,21.1406460213847,0.270833501284561));
#41135=CARTESIAN_POINT('Ctrl Pts',(-21.4140862560114,21.1371759557176,0.270513388538846));
#41136=CARTESIAN_POINT('Ctrl Pts',(-21.4203568645072,21.1316430508825,0.270000930611424));
#41137=CARTESIAN_POINT('Ctrl Pts',(-21.4227085888715,21.1295740844361,0.269808842008652));
#41138=CARTESIAN_POINT('Ctrl Pts',(-21.427558386775,21.1253199253956,0.269412921323217));
#41139=CARTESIAN_POINT('Ctrl Pts',(-21.4300568264868,21.1231351572238,0.269209071864934));
#41140=CARTESIAN_POINT('Ctrl Pts',(-21.4358200753665,21.1181111562002,0.268739105082294));
#41141=CARTESIAN_POINT('Ctrl Pts',(-21.4390872307082,21.1152746356173,0.268472875504281));
#41142=CARTESIAN_POINT('Ctrl Pts',(-21.4490648588767,21.1066473078217,0.267660409089334));
#41143=CARTESIAN_POINT('Ctrl Pts',(-21.4557934763808,21.1008776339632,0.267113298816795));
#41144=CARTESIAN_POINT('Ctrl Pts',(-21.4704117117014,21.088447027717,0.265926344719462));
#41145=CARTESIAN_POINT('Ctrl Pts',(-21.4783096919318,21.081796123191,0.265286096037397));
#41146=CARTESIAN_POINT('Ctrl Pts',(-21.687408763093,20.9074239372215,0.248362150119762));
#41147=CARTESIAN_POINT('Ctrl Pts',(-21.908234965077,20.764853068017,0.231012769475701));
#41148=CARTESIAN_POINT('Ctrl Pts',(-22.2899888093119,20.5796892126811,0.202321042049335));
#41149=CARTESIAN_POINT('Ctrl Pts',(-22.4413207811096,20.5199412724886,0.191269355035347));
#41150=CARTESIAN_POINT('Ctrl Pts',(-22.658252344682,20.4527325469802,0.176339826379156));
#41151=CARTESIAN_POINT('Ctrl Pts',(-22.7205522883347,20.4354663068507,0.172154963881771));
#41152=CARTESIAN_POINT('Ctrl Pts',(-22.79848723561,20.416371566337,0.167080893385526));
#41153=CARTESIAN_POINT('Ctrl Pts',(-22.8136675502153,20.4127688976372,0.166100067640527));
#41154=CARTESIAN_POINT('Ctrl Pts',(-22.8325087148812,20.4084417026453,0.164892510610802));
#41155=CARTESIAN_POINT('Ctrl Pts',(-22.8361451074413,20.4076131856883,0.164659900356568));
#41156=CARTESIAN_POINT('Ctrl Pts',(-22.8418767195626,20.4063177551618,0.164293984302377));
#41157=CARTESIAN_POINT('Ctrl Pts',(-22.8439709668546,20.4058466225381,0.164160435194475));
#41158=CARTESIAN_POINT('Ctrl Pts',(-22.8478875659604,20.4049696345513,0.163910960425778));
#41159=CARTESIAN_POINT('Ctrl Pts',(-22.8497097874238,20.4045632731013,0.163795006218067));
#41160=CARTESIAN_POINT('Ctrl Pts',(-22.8538031789774,20.403654166397,0.163534788016768));
#41161=CARTESIAN_POINT('Ctrl Pts',(-22.8560745359861,20.4031522975487,0.16339057542968));
#41162=CARTESIAN_POINT('Ctrl Pts',(-22.8618519881338,20.4018822966713,0.163024203188053));
#41163=CARTESIAN_POINT('Ctrl Pts',(-22.8653588372245,20.4011175595607,0.162802239307252));
#41164=CARTESIAN_POINT('Ctrl Pts',(-22.884747589944,20.3969233813881,0.161577323578932));
#41165=CARTESIAN_POINT('Ctrl Pts',(-22.9006543486063,20.3936081449619,0.160580852238311));
#41166=CARTESIAN_POINT('Ctrl Pts',(-23.2299989063664,20.3275621716161,0.140111144292248));
#41167=CARTESIAN_POINT('Ctrl Pts',(-23.5510772879119,20.3116763547085,0.123048013008246));
#41168=CARTESIAN_POINT('Ctrl Pts',(-23.9797844309823,20.3543253268618,0.098635244908576));
#41169=CARTESIAN_POINT('Ctrl Pts',(-24.0896323544244,20.3710207793976,0.0922494552223906));
#41170=CARTESIAN_POINT('Ctrl Pts',(-24.2654688057172,20.4071216074122,0.0816516820150702));
#41171=CARTESIAN_POINT('Ctrl Pts',(-24.3320841114588,20.4230261819133,0.0775482675371054));
#41172=CARTESIAN_POINT('Ctrl Pts',(-24.406372700293,20.4432847722791,0.072855041176118));
#41173=CARTESIAN_POINT('Ctrl Pts',(-24.4145975693603,20.4455628443371,0.0723338065685653));
#41174=CARTESIAN_POINT('Ctrl Pts',(-24.4268481571589,20.4490083877383,0.0715549941180591));
#41175=CARTESIAN_POINT('Ctrl Pts',(-24.4308808506585,20.4501510987441,0.0712982240746903));
#41176=CARTESIAN_POINT('Ctrl Pts',(-24.4380406120034,20.4521949987125,0.0708416358861511));
#41177=CARTESIAN_POINT('Ctrl Pts',(-24.4411685715318,20.4530930648537,0.0706419199726562));
#41178=CARTESIAN_POINT('Ctrl Pts',(-24.4477607611836,20.4549965564476,0.0702205060665057));
#41179=CARTESIAN_POINT('Ctrl Pts',(-24.4512246722264,20.456003062741,0.0699987729657552));
#41180=CARTESIAN_POINT('Ctrl Pts',(-24.4601388756374,20.4586094945502,0.0694273817279601));
#41181=CARTESIAN_POINT('Ctrl Pts',(-24.4655866240651,20.4602180130039,0.0690774426830349));
#41182=CARTESIAN_POINT('Ctrl Pts',(-24.4871992506722,20.466661590957,0.0676861664964763));
#41183=CARTESIAN_POINT('Ctrl Pts',(-24.5033300772324,20.4716090936248,0.0666411479314599));
#41184=CARTESIAN_POINT('Ctrl Pts',(-24.7810926326637,20.5591941385627,0.0485298550585272));
#41185=CARTESIAN_POINT('Ctrl Pts',(-25.0310975387023,20.6747648142353,0.0302872386054696));
#41186=CARTESIAN_POINT('Ctrl Pts',(-25.3293758929812,20.8619619106936,0.00645562504132138));
#41187=CARTESIAN_POINT('Ctrl Pts',(-25.3938377808542,20.9057525593612,0.00117653361270985));
#41188=CARTESIAN_POINT('Ctrl Pts',(-25.5434226807009,21.0154995282732,-0.0113055845170199));
#41189=CARTESIAN_POINT('Ctrl Pts',(-25.6269598786956,21.0834751391232,-0.0184678596970956));
#41190=CARTESIAN_POINT('Ctrl Pts',(-25.7279007074455,21.1743818913481,-0.0272249476669519));
#41191=CARTESIAN_POINT('Ctrl Pts',(-25.7486085929477,21.1935294616425,-0.0290271458694069));
#41192=CARTESIAN_POINT('Ctrl Pts',(-25.7804074409697,21.2237161991043,-0.0317998457133827));
#41193=CARTESIAN_POINT('Ctrl Pts',(-25.7916733587597,21.2345679836838,-0.0327832292112673));
#41194=CARTESIAN_POINT('Ctrl Pts',(-25.8055295586595,21.2481106969068,-0.0339935117048435));
#41195=CARTESIAN_POINT('Ctrl Pts',(-25.8081945091748,21.2507244230372,-0.034226321148725));
#41196=CARTESIAN_POINT('Ctrl Pts',(-25.8123853361987,21.254849005488,-0.0345924800485561));
#41197=CARTESIAN_POINT('Ctrl Pts',(-25.8139142434358,21.2563567563384,-0.0347260733503726));
#41198=CARTESIAN_POINT('Ctrl Pts',(-25.8167696111653,21.259178247359,-0.0349755878625767));
#41199=CARTESIAN_POINT('Ctrl Pts',(-25.8180964280798,21.2604916032282,-0.0350915377095388));
#41200=CARTESIAN_POINT('Ctrl Pts',(-25.8210731871779,21.2634432874672,-0.0353516912653111));
#41201=CARTESIAN_POINT('Ctrl Pts',(-25.822722494452,21.2650822454113,-0.0354958436799492));
#41202=CARTESIAN_POINT('Ctrl Pts',(-25.8269110237644,21.2692535108402,-0.0358619622122694));
#41203=CARTESIAN_POINT('Ctrl Pts',(-25.8294478030405,21.2717882818079,-0.0360837330245468));
#41204=CARTESIAN_POINT('Ctrl Pts',(-25.8434271067988,21.2858032265454,-0.037306044894854));
#41205=CARTESIAN_POINT('Ctrl Pts',(-25.8547873957157,21.297365633975,-0.0383001375012151));
#41206=CARTESIAN_POINT('Ctrl Pts',(-26.0846180650061,21.5348430468127,-0.0584402269181293));
#41207=CARTESIAN_POINT('Ctrl Pts',(-26.2690097287303,21.7914686636345,-0.0752522841314742));
#41208=CARTESIAN_POINT('Ctrl Pts',(-26.4950549821759,22.2289121301765,-0.103114262930192));
#41209=CARTESIAN_POINT('Ctrl Pts',(-26.5635170066255,22.3935221853769,-0.113423636470402));
#41210=CARTESIAN_POINT('Ctrl Pts',(-26.6221287606919,22.5756385925777,-0.12504545751006));
#41211=CARTESIAN_POINT('Ctrl Pts',(-26.6261408633413,22.588375793527,-0.125859245529396));
#41212=CARTESIAN_POINT('Ctrl Pts',(-26.6315748634349,22.6060087949187,-0.126987272201844));
#41213=CARTESIAN_POINT('Ctrl Pts',(-26.6330645207062,22.610883708252,-0.127299284210471));
#41214=CARTESIAN_POINT('Ctrl Pts',(-26.6355585478241,22.619115256608,-0.127826396334402));
#41215=CARTESIAN_POINT('Ctrl Pts',(-26.6365690244515,22.6224700439297,-0.128041295836377));
#41216=CARTESIAN_POINT('Ctrl Pts',(-26.6385567882603,22.6291086125849,-0.128466694786657));
#41217=CARTESIAN_POINT('Ctrl Pts',(-26.6395343137876,22.6323923182024,-0.128677186100811));
#41218=CARTESIAN_POINT('Ctrl Pts',(-26.6416761176096,22.6396292514416,-0.129141246939347));
#41219=CARTESIAN_POINT('Ctrl Pts',(-26.6428380519084,22.6435831619635,-0.12939489283442));
#41220=CARTESIAN_POINT('Ctrl Pts',(-26.646863658873,22.657379548205,-0.130280314817266));
#41221=CARTESIAN_POINT('Ctrl Pts',(-26.6496879310761,22.6672333706485,-0.130913376745396));
#41222=CARTESIAN_POINT('Ctrl Pts',(-26.6778635784282,22.7673383186684,-0.137351691139239));
#41223=CARTESIAN_POINT('Ctrl Pts',(-26.6993102963944,22.8586328662693,-0.143283359476885));
#41224=CARTESIAN_POINT('Ctrl Pts',(-26.735140659056,23.0478763022963,-0.155719553475827));
#41225=CARTESIAN_POINT('Ctrl Pts',(-26.7490525265102,23.1458146722644,-0.162231271757614));
#41226=CARTESIAN_POINT('Ctrl Pts',(-26.7682348801184,23.3469133100907,-0.175716306674401));
#41227=CARTESIAN_POINT('Ctrl Pts',(-26.77309380282,23.4500034301552,-0.182689934824677));
#41228=CARTESIAN_POINT('Ctrl Pts',(-26.7728461899883,23.7258964258954,-0.201365712422515));
#41229=CARTESIAN_POINT('Ctrl Pts',(-26.7588011919433,23.8983710442638,-0.213063909669046));
#41230=CARTESIAN_POINT('Ctrl Pts',(-26.7304311277122,24.0723578196513,-0.224431325583277));
#41231=CARTESIAN_POINT('Ctrl Pts',(-26.7298617210067,24.0758143622566,-0.224656975511129));
#41232=CARTESIAN_POINT('Ctrl Pts',(-26.7230044100128,24.1170221251666,-0.227344862316903));
#41233=CARTESIAN_POINT('Ctrl Pts',(-26.7160498075461,24.1546614865963,-0.229777613971489));
#41234=CARTESIAN_POINT('Ctrl Pts',(-26.7073782871479,24.1973245473106,-0.232502702669006));
#41235=CARTESIAN_POINT('Ctrl Pts',(-26.7063179754438,24.2024765306747,-0.232831244323582));
#41236=CARTESIAN_POINT('Ctrl Pts',(-26.7047476509662,24.2100131330414,-0.233311039571711));
#41237=CARTESIAN_POINT('Ctrl Pts',(-26.704247544517,24.2123997719544,-0.233462858298347));
#41238=CARTESIAN_POINT('Ctrl Pts',(-26.7033561502634,24.2166298154194,-0.233731724833956));
#41239=CARTESIAN_POINT('Ctrl Pts',(-26.702965954197,24.2184734452728,-0.233848835686228));
#41240=CARTESIAN_POINT('Ctrl Pts',(-26.702146465012,24.2223287376662,-0.234093578604118));
#41241=CARTESIAN_POINT('Ctrl Pts',(-26.7017168639319,24.224340327319,-0.234221192360505));
#41242=CARTESIAN_POINT('Ctrl Pts',(-26.7005870248269,24.2296060653125,-0.234555023295103));
#41243=CARTESIAN_POINT('Ctrl Pts',(-26.6998836683004,24.2328595532082,-0.234761060351634));
#41244=CARTESIAN_POINT('Ctrl Pts',(-26.6967792709118,24.2471124847494,-0.235662713551194));
#41245=CARTESIAN_POINT('Ctrl Pts',(-26.6943256035827,24.2581005678354,-0.2363553299075));
#41246=CARTESIAN_POINT('Ctrl Pts',(-26.6759513950936,24.3384036380501,-0.241400299574725));
#41247=CARTESIAN_POINT('Ctrl Pts',(-26.6577964796317,24.4071935558015,-0.245630292851446));
#41248=CARTESIAN_POINT('Ctrl Pts',(-26.6146562079719,24.5511589707876,-0.254396239781917));
#41249=CARTESIAN_POINT('Ctrl Pts',(-26.5891467834824,24.6261273795643,-0.258909972711792));
#41250=CARTESIAN_POINT('Ctrl Pts',(-26.4397431226913,25.0173168125652,-0.282545749088872));
#41251=CARTESIAN_POINT('Ctrl Pts',(-26.2692292869155,25.3133720586982,-0.300999264206647));
#41252=CARTESIAN_POINT('Ctrl Pts',(-26.0432001403632,25.592731654574,-0.322738542431323));
#41253=CARTESIAN_POINT('Ctrl Pts',(-26.0306185174856,25.6079923831733,-0.32394063699489));
#41254=CARTESIAN_POINT('Ctrl Pts',(-26.0139229217475,25.6278674995866,-0.325525810478143));
#41255=CARTESIAN_POINT('Ctrl Pts',(-26.009934829622,25.6325874562575,-0.325903727421661));
#41256=CARTESIAN_POINT('Ctrl Pts',(-26.0037528256426,25.6398613960511,-0.326488423432875));
#41257=CARTESIAN_POINT('Ctrl Pts',(-26.0015684294766,25.6424234777562,-0.326694810037525));
#41258=CARTESIAN_POINT('Ctrl Pts',(-25.9972064383223,25.6475234546308,-0.327106516747561));
#41259=CARTESIAN_POINT('Ctrl Pts',(-25.9950289000438,25.6500613929917,-0.327311834363868));
#41260=CARTESIAN_POINT('Ctrl Pts',(-25.9901871588031,25.6556867406035,-0.327767895325005));
#41261=CARTESIAN_POINT('Ctrl Pts',(-25.9875210412345,25.6587724876752,-0.328018717946543));
#41262=CARTESIAN_POINT('Ctrl Pts',(-25.9797939441341,25.6676815416659,-0.328744782312228));
#41263=CARTESIAN_POINT('Ctrl Pts',(-25.9747179268682,25.6734917158124,-0.329220650069114));
#41264=CARTESIAN_POINT('Ctrl Pts',(-25.9398846473205,25.7130752358933,-0.332478865905345));
#41265=CARTESIAN_POINT('Ctrl Pts',(-25.9094447675075,25.746238724928,-0.335289815172548));
#41266=CARTESIAN_POINT('Ctrl Pts',(-25.8288050456904,25.8304814154994,-0.342649284810011));
#41267=CARTESIAN_POINT('Ctrl Pts',(-25.7775816219825,25.8805420338546,-0.347241275070761));
#41268=CARTESIAN_POINT('Ctrl Pts',(-25.6140486675017,26.0300416720214,-0.361655314787619));
#41269=CARTESIAN_POINT('Ctrl Pts',(-25.4964434713283,26.1233714928482,-0.371693085323411));
#41270=CARTESIAN_POINT('Ctrl Pts',(-25.1773924521551,26.342144303118,-0.397836721284272));
#41271=CARTESIAN_POINT('Ctrl Pts',(-24.9678089969649,26.4541808049471,-0.414039348090076));
#41272=CARTESIAN_POINT('Ctrl Pts',(-24.7353086134694,26.5472412323637,-0.429850228012322));
#41273=CARTESIAN_POINT('Ctrl Pts',(-24.7227652056926,26.5521707906457,-0.430696741768996));
#41274=CARTESIAN_POINT('Ctrl Pts',(-24.7067613316152,26.5583446963806,-0.431768219570169));
#41275=CARTESIAN_POINT('Ctrl Pts',(-24.703329398214,26.5596619115826,-0.431997491654009));
#41276=CARTESIAN_POINT('Ctrl Pts',(-24.6978808305264,26.5617424452658,-0.432360684920211));
#41277=CARTESIAN_POINT('Ctrl Pts',(-24.6958656842691,26.5625096117816,-0.432494837905251));
#41278=CARTESIAN_POINT('Ctrl Pts',(-24.6921395247644,26.5639238813658,-0.432742574217777));
#41279=CARTESIAN_POINT('Ctrl Pts',(-24.6904287414695,26.5645715459103,-0.432856190966694));
#41280=CARTESIAN_POINT('Ctrl Pts',(-24.6866150365703,26.5660116185794,-0.433109187484006));
#41281=CARTESIAN_POINT('Ctrl Pts',(-24.6845118419263,26.5668032821118,-0.433248521707288));
#41282=CARTESIAN_POINT('Ctrl Pts',(-24.6801299824222,26.5684474272943,-0.433538424510278));
#41283=CARTESIAN_POINT('Ctrl Pts',(-24.6778511755879,26.5692995303135,-0.43368897025165));
#41284=CARTESIAN_POINT('Ctrl Pts',(-24.6719552802554,26.5714965467324,-0.434077910884803));
#41285=CARTESIAN_POINT('Ctrl Pts',(-24.668336723943,26.5728375501745,-0.434316073145402));
#41286=CARTESIAN_POINT('Ctrl Pts',(-24.6577395903057,26.5767431156185,-0.435011968950935));
#41287=CARTESIAN_POINT('Ctrl Pts',(-24.6507544791301,26.5792900530515,-0.43546867317455));
#41288=CARTESIAN_POINT('Ctrl Pts',(-24.5771981469014,26.6058224094536,-0.440257626357364));
#41289=CARTESIAN_POINT('Ctrl Pts',(-24.5098571976897,26.6276353794079,-0.444467007518637));
#41290=CARTESIAN_POINT('Ctrl Pts',(-24.3664640035169,26.6689173080416,-0.453172340694728));
#41291=CARTESIAN_POINT('Ctrl Pts',(-24.2903094343048,26.6878612195325,-0.457647067955348));
#41292=CARTESIAN_POINT('Ctrl Pts',(-23.8803664704533,26.7740785069709,-0.481299136526181));
#41293=CARTESIAN_POINT('Ctrl Pts',(-23.5382393407314,26.7909125068505,-0.499791292278699));
#41294=CARTESIAN_POINT('Ctrl Pts',(-23.1799547185387,26.7517203365284,-0.52159301522342));
#41295=CARTESIAN_POINT('Ctrl Pts',(-23.1601188314851,26.7493636963513,-0.522806993769418));
#41296=CARTESIAN_POINT('Ctrl Pts',(-23.1341534109168,26.7460337455871,-0.524405635664677));
#41297=CARTESIAN_POINT('Ctrl Pts',(-23.1280026723124,26.7452268822617,-0.524785026784344));
#41298=CARTESIAN_POINT('Ctrl Pts',(-23.1185124949875,26.743954063145,-0.525371498009442));
#41299=CARTESIAN_POINT('Ctrl Pts',(-23.1151713701045,26.7435006138167,-0.525578181753649));
#41300=CARTESIAN_POINT('Ctrl Pts',(-23.1085183921398,26.7425870524723,-0.525990159056699));
#41301=CARTESIAN_POINT('Ctrl Pts',(-23.105206531108,26.7421270279469,-0.526195449604739));
#41302=CARTESIAN_POINT('Ctrl Pts',(-23.0978650973423,26.7410956390393,-0.526650982364138));
#41303=CARTESIAN_POINT('Ctrl Pts',(-23.0938358838619,26.7405217945919,-0.526901302927074));
#41304=CARTESIAN_POINT('Ctrl Pts',(-23.0822095264602,26.7388434813631,-0.527624506576167));
#41305=CARTESIAN_POINT('Ctrl Pts',(-23.0746152667785,26.7377195024483,-0.528098008058565));
#41306=CARTESIAN_POINT('Ctrl Pts',(-23.0233328907344,26.7299421666856,-0.531303048318972));
#41307=CARTESIAN_POINT('Ctrl Pts',(-22.9797834165328,26.7224182206039,-0.534062133465268));
#41308=CARTESIAN_POINT('Ctrl Pts',(-22.8780061887156,26.7026708282401,-0.540602217432489));
#41309=CARTESIAN_POINT('Ctrl Pts',(-22.8199365091347,26.6897260588641,-0.544405174985379));
#41310=CARTESIAN_POINT('Ctrl Pts',(-22.6837477852807,26.6553843177723,-0.553495599609622));
#41311=CARTESIAN_POINT('Ctrl Pts',(-22.6060135927911,26.6326355583656,-0.558820276853013));
#41312=CARTESIAN_POINT('Ctrl Pts',(-22.3729489478991,26.5547858055371,-0.575171464795435));
#41313=CARTESIAN_POINT('Ctrl Pts',(-22.2211232282342,26.4907510558054,-0.586370102522171));
#41314=CARTESIAN_POINT('Ctrl Pts',(-22.0750358767111,26.4155367031789,-0.597455529348902));
#41315=CARTESIAN_POINT('',(-26.7730021510373,23.5486861587587,-0.433369846446908));
#41316=CARTESIAN_POINT('Ctrl Pts',(-22.0750363147453,26.4155369287046,-0.841310143832836));
#41317=CARTESIAN_POINT('Ctrl Pts',(-22.1918959590995,26.4757031176658,-0.832483085698408));
#41318=CARTESIAN_POINT('Ctrl Pts',(-22.3123968422096,26.5286998695453,-0.823785630732621));
#41319=CARTESIAN_POINT('Ctrl Pts',(-22.4469193609948,26.5782736674178,-0.814748539363253));
#41320=CARTESIAN_POINT('Ctrl Pts',(-22.4579852758515,26.5822829299526,-0.814009994337906));
#41321=CARTESIAN_POINT('Ctrl Pts',(-22.4723994529638,26.58741613792,-0.813054511133772));
#41322=CARTESIAN_POINT('Ctrl Pts',(-22.4757277613118,26.588595262268,-0.812834336061839));
#41323=CARTESIAN_POINT('Ctrl Pts',(-22.4808428650176,26.5903979408247,-0.812496660141599));
#41324=CARTESIAN_POINT('Ctrl Pts',(-22.4826282693482,26.5910253904148,-0.812378926626182));
#41325=CARTESIAN_POINT('Ctrl Pts',(-22.4860037179556,26.5922082943084,-0.812156590560344));
#41326=CARTESIAN_POINT('Ctrl Pts',(-22.4875936376374,26.5927640722077,-0.812051969046023));
#41327=CARTESIAN_POINT('Ctrl Pts',(-22.4912258690637,26.5940305732807,-0.811813195049276));
#41328=CARTESIAN_POINT('Ctrl Pts',(-22.4932684569645,26.5947404860865,-0.811679091665356));
#41329=CARTESIAN_POINT('Ctrl Pts',(-22.4989641769027,26.5967136423387,-0.811305620165246));
#41330=CARTESIAN_POINT('Ctrl Pts',(-22.5026188848862,26.5979723754523,-0.811066521380125));
#41331=CARTESIAN_POINT('Ctrl Pts',(-22.5107813783029,26.600767236343,-0.810533705104373));
#41332=CARTESIAN_POINT('Ctrl Pts',(-22.5152903329119,26.6022999575678,-0.810240187568537));
#41333=CARTESIAN_POINT('Ctrl Pts',(-22.5291937717427,26.6069917758105,-0.809337566395588));
#41334=CARTESIAN_POINT('Ctrl Pts',(-22.5385995513683,26.6101175697421,-0.808730371139305));
#41335=CARTESIAN_POINT('Ctrl Pts',(-22.5734856241607,26.6215327072147,-0.806490462878175));
#41336=CARTESIAN_POINT('Ctrl Pts',(-22.5990553661165,26.6295478349863,-0.804872722669587));
#41337=CARTESIAN_POINT('Ctrl Pts',(-22.6897370908625,26.6567356745358,-0.799210185580214));
#41338=CARTESIAN_POINT('Ctrl Pts',(-22.7553552489818,26.6741705685107,-0.795247710534378));
#41339=CARTESIAN_POINT('Ctrl Pts',(-23.2029480943067,26.7780781123869,-0.768826597802522));
#41340=CARTESIAN_POINT('Ctrl Pts',(-23.5973444654112,26.7963734817766,-0.748049077700995));
#41341=CARTESIAN_POINT('Ctrl Pts',(-24.004569985287,26.7408773391201,-0.723179021927088));
#41342=CARTESIAN_POINT('Ctrl Pts',(-24.0236936060035,26.738095773486,-0.722004304385006));
#41343=CARTESIAN_POINT('Ctrl Pts',(-24.0488417516076,26.734206652401,-0.720450186398075));
#41344=CARTESIAN_POINT('Ctrl Pts',(-24.0548900552158,26.7332536347439,-0.720075698370171));
#41345=CARTESIAN_POINT('Ctrl Pts',(-24.0642488285811,26.7317516484153,-0.719495124017312));
#41346=CARTESIAN_POINT('Ctrl Pts',(-24.0675612412363,26.7312147323194,-0.719289421140707));
#41347=CARTESIAN_POINT('Ctrl Pts',(-24.0738440823315,26.7301862598864,-0.718898839913368));
#41348=CARTESIAN_POINT('Ctrl Pts',(-24.0768146742458,26.7296957121158,-0.718713993839199));
#41349=CARTESIAN_POINT('Ctrl Pts',(-24.0836841870394,26.7285514258461,-0.718286128660739));
#41350=CARTESIAN_POINT('Ctrl Pts',(-24.087582595005,26.7278946755377,-0.718043013917701));
#41351=CARTESIAN_POINT('Ctrl Pts',(-24.0985144021371,26.7260323424104,-0.717360420663766));
#41352=CARTESIAN_POINT('Ctrl Pts',(-24.1055449879307,26.7248105751813,-0.716920427092435));
#41353=CARTESIAN_POINT('Ctrl Pts',(-24.1463156897247,26.7175859062542,-0.714363037019959));
#41354=CARTESIAN_POINT('Ctrl Pts',(-24.17996133793,26.7110686710813,-0.712229287059696));
#41355=CARTESIAN_POINT('Ctrl Pts',(-24.2768422934146,26.6906944038584,-0.706015222023742));
#41356=CARTESIAN_POINT('Ctrl Pts',(-24.3397692170871,26.6754677680556,-0.701891876686825));
#41357=CARTESIAN_POINT('Ctrl Pts',(-24.5716825349564,26.6118997727916,-0.686363409808072));
#41358=CARTESIAN_POINT('Ctrl Pts',(-24.7370689247855,26.551661505447,-0.674603697452908));
#41359=CARTESIAN_POINT('Ctrl Pts',(-24.9650191426792,26.4468379667959,-0.65763781899987));
#41360=CARTESIAN_POINT('Ctrl Pts',(-25.0322160082494,26.41304069718,-0.65253955888881));
#41361=CARTESIAN_POINT('Ctrl Pts',(-25.1898793976965,26.3267024649186,-0.640411923944332));
#41362=CARTESIAN_POINT('Ctrl Pts',(-25.2790978469107,26.2720437575327,-0.633411823862365));
#41363=CARTESIAN_POINT('Ctrl Pts',(-25.3753922565699,26.2064011899725,-0.625814748918397));
#41364=CARTESIAN_POINT('Ctrl Pts',(-25.3852407423554,26.1996069785357,-0.625037279936702));
#41365=CARTESIAN_POINT('Ctrl Pts',(-25.3966811073754,26.1916201752299,-0.624133784990768));
#41366=CARTESIAN_POINT('Ctrl Pts',(-25.3983098616422,26.1904808586814,-0.62400514673842));
#41367=CARTESIAN_POINT('Ctrl Pts',(-25.4037912926175,26.1866390304628,-0.62357219995578));
#41368=CARTESIAN_POINT('Ctrl Pts',(-25.4076391223868,26.1839295738487,-0.623268238767382));
#41369=CARTESIAN_POINT('Ctrl Pts',(-25.4135267678604,26.1797644565317,-0.622803091602461));
#41370=CARTESIAN_POINT('Ctrl Pts',(-25.4155708275809,26.1783148401515,-0.622641593623739));
#41371=CARTESIAN_POINT('Ctrl Pts',(-25.4498287265583,26.1539595511138,-0.619934803102744));
#41372=CARTESIAN_POINT('Ctrl Pts',(-25.4816220249929,26.1304641892959,-0.617420831748965));
#41373=CARTESIAN_POINT('Ctrl Pts',(-25.5171873745454,26.103155402757,-0.614613886052682));
#41374=CARTESIAN_POINT('Ctrl Pts',(-25.5213900531472,26.0999118457169,-0.614282281215068));
#41375=CARTESIAN_POINT('Ctrl Pts',(-25.5275188083326,26.095157564381,-0.613798852146006));
#41376=CARTESIAN_POINT('Ctrl Pts',(-25.529451181003,26.0936550285076,-0.613646450621238));
#41377=CARTESIAN_POINT('Ctrl Pts',(-25.5328693675954,26.0909909285638,-0.613376908017485));
#41378=CARTESIAN_POINT('Ctrl Pts',(-25.534355874656,26.0898302611304,-0.613259702829827));
#41379=CARTESIAN_POINT('Ctrl Pts',(-25.5372174959365,26.0875918558252,-0.613034103258723));
#41380=CARTESIAN_POINT('Ctrl Pts',(-25.5385927478522,26.0865143083552,-0.612925695762816));
#41381=CARTESIAN_POINT('Ctrl Pts',(-25.5422968310571,26.0836071935239,-0.612633743570966));
#41382=CARTESIAN_POINT('Ctrl Pts',(-25.5446240250329,26.0817755278301,-0.612450349458289));
#41383=CARTESIAN_POINT('Ctrl Pts',(-25.5534476327734,26.0748110077101,-0.611755117886821));
#41384=CARTESIAN_POINT('Ctrl Pts',(-25.5599268563628,26.0696562754687,-0.611244834929675));
#41385=CARTESIAN_POINT('Ctrl Pts',(-25.576004838508,26.0567634858304,-0.609978953580685));
#41386=CARTESIAN_POINT('Ctrl Pts',(-25.585579285352,26.0489951332312,-0.609225450444682));
#41387=CARTESIAN_POINT('Ctrl Pts',(-25.6230091478245,26.0182680445942,-0.606279984041182));
#41388=CARTESIAN_POINT('Ctrl Pts',(-25.6505237344633,25.9948959982704,-0.604115303526411));
#41389=CARTESIAN_POINT('Ctrl Pts',(-25.7261447007332,25.9284409778457,-0.598148569295593));
#41390=CARTESIAN_POINT('Ctrl Pts',(-25.7733592726218,25.8843657294892,-0.594402894442797));
#41391=CARTESIAN_POINT('Ctrl Pts',(-26.0062861855531,25.6534416356921,-0.575627077735363));
#41392=CARTESIAN_POINT('Ctrl Pts',(-26.169911070631,25.445748978468,-0.561351382405291));
#41393=CARTESIAN_POINT('Ctrl Pts',(-26.3335894777414,25.1756440581429,-0.543184384200481));
#41394=CARTESIAN_POINT('Ctrl Pts',(-26.3596425931045,25.1301858429121,-0.540142650404));
#41395=CARTESIAN_POINT('Ctrl Pts',(-26.3886519017998,25.0765814417388,-0.53656234992002));
#41396=CARTESIAN_POINT('Ctrl Pts',(-26.3926984385456,25.0690323678068,-0.536058291059274));
#41397=CARTESIAN_POINT('Ctrl Pts',(-26.4295299396103,24.9996580601409,-0.531427153743921));
#41398=CARTESIAN_POINT('Ctrl Pts',(-26.4603210531502,24.9368003484797,-0.527238064177088));
#41399=CARTESIAN_POINT('Ctrl Pts',(-26.4929304955564,24.8643506253012,-0.522398981515381));
#41400=CARTESIAN_POINT('Ctrl Pts',(-26.4967825305603,24.8556905276877,-0.521820393960499));
#41401=CARTESIAN_POINT('Ctrl Pts',(-26.5023613613589,24.8429977745731,-0.520972104266465));
#41402=CARTESIAN_POINT('Ctrl Pts',(-26.5041182399141,24.8389783297875,-0.520703433809886));
#41403=CARTESIAN_POINT('Ctrl Pts',(-26.5072167905813,24.831849738715,-0.520226863002594));
#41404=CARTESIAN_POINT('Ctrl Pts',(-26.5085617817672,24.8287420350426,-0.520019076569772));
#41405=CARTESIAN_POINT('Ctrl Pts',(-26.5113443834544,24.8222847225499,-0.519587273469587));
#41406=CARTESIAN_POINT('Ctrl Pts',(-26.5127812134829,24.8189347844821,-0.519363230504296));
#41407=CARTESIAN_POINT('Ctrl Pts',(-26.5164698165109,24.8102944518615,-0.518785283022863));
#41408=CARTESIAN_POINT('Ctrl Pts',(-26.5187131134266,24.8050004726527,-0.518431090052694));
#41409=CARTESIAN_POINT('Ctrl Pts',(-26.5280007512499,24.782918169432,-0.51695331458252));
#41410=CARTESIAN_POINT('Ctrl Pts',(-26.5349168229369,24.7660765651026,-0.515825380618384));
#41411=CARTESIAN_POINT('Ctrl Pts',(-26.6552803236543,24.4657576550718,-0.495693907005689));
#41412=CARTESIAN_POINT('Ctrl Pts',(-26.7279911436311,24.167694796446,-0.475200616383863));
#41413=CARTESIAN_POINT('Ctrl Pts',(-26.7679455708432,23.759182062243,-0.447428429760582));
#41414=CARTESIAN_POINT('Ctrl Pts',(-26.7730533208591,23.6539660190022,-0.440326684895173));
#41415=CARTESIAN_POINT('Ctrl Pts',(-26.7730021510373,23.5486861587587,-0.433369846446908));
#41416=CARTESIAN_POINT('Ctrl Pts',(-26.773002148774,23.5486815090728,-0.433369539198178));
#41417=CARTESIAN_POINT('Ctrl Pts',(-26.7729606909923,23.4636362345256,-0.427749795259021));
#41418=CARTESIAN_POINT('Ctrl Pts',(-26.7695528295525,23.3786153665292,-0.422229805789728));
#41419=CARTESIAN_POINT('Ctrl Pts',(-26.7624563038197,23.2897118072575,-0.416627183339296));
#41420=CARTESIAN_POINT('Ctrl Pts',(-26.7621205403511,23.2856047692772,-0.416368743239842));
#41421=CARTESIAN_POINT('Ctrl Pts',(-26.7614599942432,23.2777114595341,-0.415872796195772));
#41422=CARTESIAN_POINT('Ctrl Pts',(-26.7611363903938,23.273925099402,-0.41563522544598));
#41423=CARTESIAN_POINT('Ctrl Pts',(-26.7605967693513,23.267740164003,-0.415247709940809));
#41424=CARTESIAN_POINT('Ctrl Pts',(-26.7603847606628,23.2653412564105,-0.41509754249434));
#41425=CARTESIAN_POINT('Ctrl Pts',(-26.7600056746364,23.2611059875934,-0.414832663968443));
#41426=CARTESIAN_POINT('Ctrl Pts',(-26.7598397101878,23.2592695317042,-0.414717890268604));
#41427=CARTESIAN_POINT('Ctrl Pts',(-26.7595092345212,23.255647383065,-0.414491675273463));
#41428=CARTESIAN_POINT('Ctrl Pts',(-26.7593448087476,23.253861682207,-0.414380229125421));
#41429=CARTESIAN_POINT('Ctrl Pts',(-26.7590137519495,23.2502989025832,-0.414158028929345));
#41430=CARTESIAN_POINT('Ctrl Pts',(-26.7588471354849,23.2485218292531,-0.414047274311157));
#41431=CARTESIAN_POINT('Ctrl Pts',(-26.7584439880963,23.2442600954756,-0.413781846279013));
#41432=CARTESIAN_POINT('Ctrl Pts',(-26.7582060464848,23.2417755649755,-0.413627253059689));
#41433=CARTESIAN_POINT('Ctrl Pts',(-26.7574718173178,23.2342016425685,-0.413156429265943));
#41434=CARTESIAN_POINT('Ctrl Pts',(-26.7569662998405,23.2291131217427,-0.412840717630414));
#41435=CARTESIAN_POINT('Ctrl Pts',(-26.7513427504129,23.1738441942195,-0.409418039451498));
#41436=CARTESIAN_POINT('Ctrl Pts',(-26.7450590604961,23.1237859262715,-0.406375555810663));
#41437=CARTESIAN_POINT('Ctrl Pts',(-26.7370975668604,23.070515160457,-0.403179706209221));
#41438=CARTESIAN_POINT('Ctrl Pts',(-26.7365874464137,23.06713863731,-0.402977320370541));
#41439=CARTESIAN_POINT('Ctrl Pts',(-26.7340947702606,23.0508151313361,-0.401999748975227));
#41440=CARTESIAN_POINT('Ctrl Pts',(-26.7320386390126,23.037879333752,-0.401227630439692));
#41441=CARTESIAN_POINT('Ctrl Pts',(-26.7275356033897,23.0106221784376,-0.399605448785137));
#41442=CARTESIAN_POINT('Ctrl Pts',(-26.7250705988577,22.9963040789598,-0.398756099422074));
#41443=CARTESIAN_POINT('Ctrl Pts',(-26.7202797440528,22.9695591073477,-0.397173981295573));
#41444=CARTESIAN_POINT('Ctrl Pts',(-26.7179774418262,22.9571283616891,-0.396440412217942));
#41445=CARTESIAN_POINT('Ctrl Pts',(-26.6665346735377,22.6882212334434,-0.380604037349782));
#41446=CARTESIAN_POINT('Ctrl Pts',(-26.5864733051594,22.4386342469413,-0.366468616055812));
#41447=CARTESIAN_POINT('Ctrl Pts',(-26.4314585396456,22.1022559708833,-0.345342863188886));
#41448=CARTESIAN_POINT('Ctrl Pts',(-26.380747996997,22.0054761354431,-0.339007479498481));
#41449=CARTESIAN_POINT('Ctrl Pts',(-26.3002746763841,21.8692101003068,-0.329577500096659));
#41450=CARTESIAN_POINT('Ctrl Pts',(-26.274361485691,21.8275350686512,-0.326620909519834));
#41451=CARTESIAN_POINT('Ctrl Pts',(-26.2431884874025,21.7798639322464,-0.323147545779706));
#41452=CARTESIAN_POINT('Ctrl Pts',(-26.2388447515165,21.7732742739868,-0.322665353759454));
#41453=CARTESIAN_POINT('Ctrl Pts',(-26.2321991935727,21.7632727881937,-0.321930331658308));
#41454=CARTESIAN_POINT('Ctrl Pts',(-26.2299149478962,21.7598492710331,-0.321678164530393));
#41455=CARTESIAN_POINT('Ctrl Pts',(-26.2259399757596,21.7539164218641,-0.321240175141211));
#41456=CARTESIAN_POINT('Ctrl Pts',(-26.2242522578145,21.7514050722311,-0.321054466839019));
#41457=CARTESIAN_POINT('Ctrl Pts',(-26.2207355309599,21.7461880153082,-0.320668032431311));
#41458=CARTESIAN_POINT('Ctrl Pts',(-26.218905941577,21.7434827050592,-0.320467284451658));
#41459=CARTESIAN_POINT('Ctrl Pts',(-26.214434354981,21.736892432846,-0.319977365930073));
#41460=CARTESIAN_POINT('Ctrl Pts',(-26.2117879740945,21.7330104663354,-0.319688028948727));
#41461=CARTESIAN_POINT('Ctrl Pts',(-26.2017222860675,21.7183142965163,-0.318589799752796));
#41462=CARTESIAN_POINT('Ctrl Pts',(-26.1942455597744,21.7075397447535,-0.317778719778919));
#41463=CARTESIAN_POINT('Ctrl Pts',(-26.0641342240194,21.5224612402907,-0.303743093236472));
#41464=CARTESIAN_POINT('Ctrl Pts',(-25.924598474026,21.3607348650812,-0.289834077523667));
#41465=CARTESIAN_POINT('Ctrl Pts',(-25.6523232109758,21.102021266223,-0.264621249295177));
#41466=CARTESIAN_POINT('Ctrl Pts',(-25.5261930773607,20.9991360683353,-0.25353197399763));
#41467=CARTESIAN_POINT('Ctrl Pts',(-25.3336111082468,20.8649291343552,-0.237806305414943));
#41468=CARTESIAN_POINT('Ctrl Pts',(-25.2730066683117,20.825651823641,-0.233015969421886));
#41469=CARTESIAN_POINT('Ctrl Pts',(-25.1768891738189,20.7678493798572,-0.225714613407133));
#41470=CARTESIAN_POINT('Ctrl Pts',(-25.1422659163654,20.7478949923283,-0.223141795897741));
#41471=CARTESIAN_POINT('Ctrl Pts',(-25.0956483341677,20.7221708794438,-0.219762057008459));
#41472=CARTESIAN_POINT('Ctrl Pts',(-25.0839780860035,20.7158249076009,-0.21892289988479));
#41473=CARTESIAN_POINT('Ctrl Pts',(-25.0645224101568,20.7054007731002,-0.217535818154493));
#41474=CARTESIAN_POINT('Ctrl Pts',(-25.056759064754,20.7012820398612,-0.216985456570053));
#41475=CARTESIAN_POINT('Ctrl Pts',(-25.046300475251,20.6957880869343,-0.216248310113245));
#41476=CARTESIAN_POINT('Ctrl Pts',(-25.0436200959089,20.6943848817233,-0.216059767711152));
#41477=CARTESIAN_POINT('Ctrl Pts',(-25.0393871947932,20.6921765046775,-0.21576261785026));
#41478=CARTESIAN_POINT('Ctrl Pts',(-25.0378359954855,20.6913688230869,-0.215653850439024));
#41479=CARTESIAN_POINT('Ctrl Pts',(-25.0346161893533,20.6896956580052,-0.215428347513663));
#41480=CARTESIAN_POINT('Ctrl Pts',(-25.0329474943046,20.6888303776502,-0.215311625825309));
#41481=CARTESIAN_POINT('Ctrl Pts',(-25.029142425741,20.6868615305094,-0.21504580351432));
#41482=CARTESIAN_POINT('Ctrl Pts',(-25.0270055762432,20.6857588958336,-0.214896762760868));
#41483=CARTESIAN_POINT('Ctrl Pts',(-25.0203483191145,20.6823331169821,-0.214433172708095));
#41484=CARTESIAN_POINT('Ctrl Pts',(-25.0158236203729,20.6800182593149,-0.214119147782663));
#41485=CARTESIAN_POINT('Ctrl Pts',(-24.9809757812688,20.6622938252583,-0.211708627685704));
#41486=CARTESIAN_POINT('Ctrl Pts',(-24.9504144273922,20.6473537394199,-0.209641156124055));
#41487=CARTESIAN_POINT('Ctrl Pts',(-24.9130350509513,20.6298083367712,-0.207161627785425));
#41488=CARTESIAN_POINT('Ctrl Pts',(-24.9064387967506,20.6267393528503,-0.206725910309519));
#41489=CARTESIAN_POINT('Ctrl Pts',(-24.8968915329486,20.6223366434032,-0.206097837133921));
#41490=CARTESIAN_POINT('Ctrl Pts',(-24.8939488657874,20.6209850105352,-0.205904604130387));
#41491=CARTESIAN_POINT('Ctrl Pts',(-24.8647444577383,20.6076240398141,-0.203990313010486));
#41492=CARTESIAN_POINT('Ctrl Pts',(-24.8383236295131,20.5959633755776,-0.202286070668944));
#41493=CARTESIAN_POINT('Ctrl Pts',(-24.6717886517483,20.5251231687292,-0.191694371882658));
#41494=CARTESIAN_POINT('Ctrl Pts',(-24.5277773461167,20.4755649326542,-0.183190617012992));
#41495=CARTESIAN_POINT('Ctrl Pts',(-24.3637953957064,20.4318274357486,-0.173706233545412));
#41496=CARTESIAN_POINT('Ctrl Pts',(-24.3467599656239,20.4274328157201,-0.172723371866494));
#41497=CARTESIAN_POINT('Ctrl Pts',(-24.3100304817221,20.418277833018,-0.170608138082399));
#41498=CARTESIAN_POINT('Ctrl Pts',(-24.2903258211528,20.4135632627511,-0.169475741220546));
#41499=CARTESIAN_POINT('Ctrl Pts',(-24.2474521189368,20.4037317182041,-0.167015028185077));
#41500=CARTESIAN_POINT('Ctrl Pts',(-24.2242684329288,20.3986841841782,-0.165686411223758));
#41501=CARTESIAN_POINT('Ctrl Pts',(-24.1731280777455,20.3881400573309,-0.162756943887326));
#41502=CARTESIAN_POINT('Ctrl Pts',(-24.1451501082827,20.3827572922396,-0.16115512864134));
#41503=CARTESIAN_POINT('Ctrl Pts',(-24.0819507219637,20.371465050308,-0.157533556835172));
#41504=CARTESIAN_POINT('Ctrl Pts',(-24.0466953394981,20.3657686994227,-0.155511021752524));
#41505=CARTESIAN_POINT('Ctrl Pts',(-23.8996681658487,20.3445138513874,-0.147049929284097));
#41506=CARTESIAN_POINT('Ctrl Pts',(-23.7872220803534,20.3342467008128,-0.14051203952232));
#41507=CARTESIAN_POINT('Ctrl Pts',(-23.6245140591477,20.3279703070119,-0.130813876715079));
#41508=CARTESIAN_POINT('Ctrl Pts',(-23.5745159432577,20.3272060889082,-0.127802091865754));
#41509=CARTESIAN_POINT('Ctrl Pts',(-23.5165920601263,20.3276685641337,-0.124269864390859));
#41510=CARTESIAN_POINT('Ctrl Pts',(-23.5086621305321,20.3277611520187,-0.123785363146156));
#41511=CARTESIAN_POINT('Ctrl Pts',(-23.4966095657719,20.327946370141,-0.123047537720698));
#41512=CARTESIAN_POINT('Ctrl Pts',(-23.4924865933205,20.328017645363,-0.122794884309092));
#41513=CARTESIAN_POINT('Ctrl Pts',(-23.4850173546148,20.3281611088923,-0.122336705278238));
#41514=CARTESIAN_POINT('Ctrl Pts',(-23.4816710373251,20.3282305976105,-0.12213126472485));
#41515=CARTESIAN_POINT('Ctrl Pts',(-23.4749845096964,20.3283798695983,-0.121720415824829));
#41516=CARTESIAN_POINT('Ctrl Pts',(-23.4716443029979,20.3284596345413,-0.121515008301901));
#41517=CARTESIAN_POINT('Ctrl Pts',(-23.4622551133315,20.3286984606867,-0.120937132145645));
#41518=CARTESIAN_POINT('Ctrl Pts',(-23.4562064690344,20.3288693636494,-0.120564292006981));
#41519=CARTESIAN_POINT('Ctrl Pts',(-23.4314057136373,20.329640012593,-0.119033225328796));
#41520=CARTESIAN_POINT('Ctrl Pts',(-23.4126588266654,20.3303864610752,-0.117870400155611));
#41521=CARTESIAN_POINT('Ctrl Pts',(-23.0819183389212,20.3464492935671,-0.0972554456065239));
#41522=CARTESIAN_POINT('Ctrl Pts',(-22.7738440469038,20.4068806787888,-0.0762363995151968));
#41523=CARTESIAN_POINT('Ctrl Pts',(-22.3796152857574,20.5457705854012,-0.0479704283915766));
#41524=CARTESIAN_POINT('Ctrl Pts',(-22.2816469566217,20.5858055874663,-0.0408486610661869));
#41525=CARTESIAN_POINT('Ctrl Pts',(-22.13592105616,20.6539069480672,-0.0302591077162034));
#41526=CARTESIAN_POINT('Ctrl Pts',(-22.0866246376019,20.6785029892014,-0.0266780766157556));
#41527=CARTESIAN_POINT('Ctrl Pts',(-22.0221187322504,20.7127805459983,-0.0220164701104062));
#41528=CARTESIAN_POINT('Ctrl Pts',(-22.0063278487092,20.7213416483775,-0.0208773052456294));
#41529=CARTESIAN_POINT('Ctrl Pts',(-21.9841472163808,20.7336080337546,-0.0192808708216959));
#41530=CARTESIAN_POINT('Ctrl Pts',(-21.9776977003706,20.7372037600922,-0.0188171159473739));
#41531=CARTESIAN_POINT('Ctrl Pts',(-21.9679131029038,20.7427030237857,-0.0181142938672159));
#41532=CARTESIAN_POINT('Ctrl Pts',(-21.9645690242909,20.7445903777682,-0.0178742230540317));
#41533=CARTESIAN_POINT('Ctrl Pts',(-21.9583909345512,20.7480917842342,-0.0174309557304598));
#41534=CARTESIAN_POINT('Ctrl Pts',(-21.9555559902542,20.7497041675325,-0.0172276535590465));
#41535=CARTESIAN_POINT('Ctrl Pts',(-21.9509720257329,20.7523205288224,-0.0168990924890992));
#41536=CARTESIAN_POINT('Ctrl Pts',(-21.9492215008824,20.7533218446958,-0.0167736613907947));
#41537=CARTESIAN_POINT('Ctrl Pts',(-21.9458372213183,20.7552619011751,-0.0165312450178589));
#41538=CARTESIAN_POINT('Ctrl Pts',(-21.9442033549815,20.7562004285914,-0.0164142468032592));
#41539=CARTESIAN_POINT('Ctrl Pts',(-21.940458775714,20.7583557640099,-0.0161461848339086));
#41540=CARTESIAN_POINT('Ctrl Pts',(-21.9383486140854,20.7595735356987,-0.0159951840417283));
#41541=CARTESIAN_POINT('Ctrl Pts',(-21.9316972056332,20.7634221165197,-0.0155193953020725));
#41542=CARTESIAN_POINT('Ctrl Pts',(-21.9271609735171,20.7660616436338,-0.0151951722920524));
#41543=CARTESIAN_POINT('Ctrl Pts',(-21.8898657684265,20.7878849740743,-0.0125315278559098));
#41544=CARTESIAN_POINT('Ctrl Pts',(-21.8574399267222,20.8076361675548,-0.0102283556399859));
#41545=CARTESIAN_POINT('Ctrl Pts',(-21.819503377101,20.8316732807122,-0.00753963268260769));
#41546=CARTESIAN_POINT('Ctrl Pts',(-21.8136497730548,20.8354087718558,-0.00712493104132523));
#41547=CARTESIAN_POINT('Ctrl Pts',(-21.8036174787606,20.8418566279417,-0.00641439455479403));
#41548=CARTESIAN_POINT('Ctrl Pts',(-21.7994329454138,20.8445598003436,-0.00611808735559252));
#41549=CARTESIAN_POINT('Ctrl Pts',(-21.5738929028098,20.9909990317915,0.00985002264757228));
#41550=CARTESIAN_POINT('Ctrl Pts',(-21.3709980081448,21.1613904828752,0.0241573078071055));
#41551=CARTESIAN_POINT('Ctrl Pts',(-21.0907964774909,21.4624578097231,0.0473488945240556));
#41552=CARTESIAN_POINT('Ctrl Pts',(-20.9979720108129,21.5770146053482,0.0557917091615164));
#41553=CARTESIAN_POINT('Ctrl Pts',(-20.8829194181258,21.7407646519255,0.0676947697538534));
#41554=CARTESIAN_POINT('Ctrl Pts',(-20.8535976927702,21.7847598226973,0.070876619068553));
#41555=CARTESIAN_POINT('Ctrl Pts',(-20.821078358248,21.8362541157659,0.0745900659921645));
#41556=CARTESIAN_POINT('Ctrl Pts',(-20.8168097194374,21.8430698733111,0.0750813585106056));
#41557=CARTESIAN_POINT('Ctrl Pts',(-20.8103786900877,21.8534242870177,0.0758274228257293));
#41558=CARTESIAN_POINT('Ctrl Pts',(-20.8081975228632,21.8569512920616,0.0760815006210693));
#41559=CARTESIAN_POINT('Ctrl Pts',(-20.8042834168736,21.8633078993222,0.0765393262519748));
#41560=CARTESIAN_POINT('Ctrl Pts',(-20.8025480261164,21.8661359911502,0.0767429833833166));
#41561=CARTESIAN_POINT('Ctrl Pts',(-20.7988307736843,21.8722148779074,0.0771806708958416));
#41562=CARTESIAN_POINT('Ctrl Pts',(-20.7968503004982,21.8754665122208,0.077414751914649));
#41563=CARTESIAN_POINT('Ctrl Pts',(-20.7915171513188,21.8842577563836,0.0780475170327083));
#41564=CARTESIAN_POINT('Ctrl Pts',(-20.788175414122,21.889803951972,0.0784466014257982));
#41565=CARTESIAN_POINT('Ctrl Pts',(-20.7734007251989,21.9144931439497,0.080222682535859));
#41566=CARTESIAN_POINT('Ctrl Pts',(-20.7621501275273,21.9337440493622,0.0816063142241604));
#41567=CARTESIAN_POINT('Ctrl Pts',(-20.7448461812775,21.9640709423421,0.0837845240337787));
#41568=CARTESIAN_POINT('Ctrl Pts',(-20.7386564549625,21.9750686315261,0.0845741210455968));
#41569=CARTESIAN_POINT('Ctrl Pts',(-20.7259931352688,21.9978808269861,0.0862114097813076));
#41570=CARTESIAN_POINT('Ctrl Pts',(-20.7195287177338,22.0097001216532,0.0870594082772526));
#41571=CARTESIAN_POINT('Ctrl Pts',(-20.712497128932,22.0227501042612,0.0879954132689088));
#41572=CARTESIAN_POINT('Ctrl Pts',(-20.7118563350316,22.0239411537368,0.0880808381641459));
#41573=CARTESIAN_POINT('Ctrl Pts',(-20.707933641809,22.0312433127476,0.0886045501617664));
#41574=CARTESIAN_POINT('Ctrl Pts',(-20.7046707499575,22.0373645644977,0.0890434979533087));
#41575=CARTESIAN_POINT('Ctrl Pts',(-20.6995482469145,22.0470496836921,0.0897379029601386));
#41576=CARTESIAN_POINT('Ctrl Pts',(-20.6976754845388,22.0506066030456,0.0899929054607688));
#41577=CARTESIAN_POINT('Ctrl Pts',(-20.6939370407133,22.0577393338602,0.0905042220648665));
#41578=CARTESIAN_POINT('Ctrl Pts',(-20.692071407356,22.0613151623035,0.090760537242487));
#41579=CARTESIAN_POINT('Ctrl Pts',(-20.6878847249044,22.0693765716923,0.0913383314264424));
#41580=CARTESIAN_POINT('Ctrl Pts',(-20.6855675015034,22.0738641181666,0.0916599394286235));
#41581=CARTESIAN_POINT('Ctrl Pts',(-20.6738016872162,22.096781840704,0.0933022159163836));
#41582=CARTESIAN_POINT('Ctrl Pts',(-20.6645205345106,22.1152970203391,0.094628475933402));
#41583=CARTESIAN_POINT('Ctrl Pts',(-20.523244912024,22.4040453799413,0.115303911667138));
#41584=CARTESIAN_POINT('Ctrl Pts',(-20.4295517822895,22.6913395638239,0.135972502017653));
#41585=CARTESIAN_POINT('Ctrl Pts',(-20.3619476365231,23.0724483536035,0.161869770918256));
#41586=CARTESIAN_POINT('Ctrl Pts',(-20.3502815014377,23.1581138480114,0.167581050839779));
#41587=CARTESIAN_POINT('Ctrl Pts',(-20.3395303333145,23.2707943782117,0.174868411042409));
#41588=CARTESIAN_POINT('Ctrl Pts',(-20.3373201185951,23.2974694025967,0.176577079332786));
#41589=CARTESIAN_POINT('Ctrl Pts',(-20.3347476705051,23.3340486382462,0.178894817366914));
#41590=CARTESIAN_POINT('Ctrl Pts',(-20.3340984681964,23.3439307401517,0.179518437653203));
#41591=CARTESIAN_POINT('Ctrl Pts',(-20.3332047175873,23.3585663916606,0.180438133814038));
#41592=CARTESIAN_POINT('Ctrl Pts',(-20.3329251380838,23.3633176298209,0.180736090488942));
#41593=CARTESIAN_POINT('Ctrl Pts',(-20.3324378965027,23.371922969269,0.181274620044712));
#41594=CARTESIAN_POINT('Ctrl Pts',(-20.3322266314391,23.3757768458631,0.181515391174598));
#41595=CARTESIAN_POINT('Ctrl Pts',(-20.3319077776034,23.381791009188,0.181890480235989));
#41596=CARTESIAN_POINT('Ctrl Pts',(-20.3317954402618,23.3839510241149,0.182025065213579));
#41597=CARTESIAN_POINT('Ctrl Pts',(-20.3315995171785,23.3877927832435,0.182264202151406));
#41598=CARTESIAN_POINT('Ctrl Pts',(-20.3315150752614,23.3894744725308,0.182368802204134));
#41599=CARTESIAN_POINT('Ctrl Pts',(-20.3313244664818,23.3933308506801,0.182608484144308));
#41600=CARTESIAN_POINT('Ctrl Pts',(-20.3312191856129,23.3955055773835,0.182743515185539));
#41601=CARTESIAN_POINT('Ctrl Pts',(-20.3309378137523,23.4014422743092,0.183111772550395));
#41602=CARTESIAN_POINT('Ctrl Pts',(-20.3307661123531,23.405204464204,0.183344751043484));
#41603=CARTESIAN_POINT('Ctrl Pts',(-20.3299708669236,23.4233267204072,0.184465140923115));
#41604=CARTESIAN_POINT('Ctrl Pts',(-20.329436789307,23.4376908427062,0.185347580614001));
#41605=CARTESIAN_POINT('Ctrl Pts',(-20.3184934158106,23.7966875769334,0.207272649390551));
#41606=CARTESIAN_POINT('Ctrl Pts',(-20.3633561116702,24.14083594934,0.225500527842729));
#41607=CARTESIAN_POINT('Ctrl Pts',(-20.4930395730555,24.5756311930454,0.251384422218675));
#41608=CARTESIAN_POINT('Ctrl Pts',(-20.5293895033194,24.678231105532,0.257696928091187));
#41609=CARTESIAN_POINT('Ctrl Pts',(-20.5895216358816,24.8240609966413,0.26709680078661));
#41610=CARTESIAN_POINT('Ctrl Pts',(-20.609217217609,24.86889817206,0.270047325149324));
#41611=CARTESIAN_POINT('Ctrl Pts',(-20.6332621021985,24.9204155227757,0.273514217745747));
#41612=CARTESIAN_POINT('Ctrl Pts',(-20.6366245559732,24.9275512666281,0.273996152668289));
#41613=CARTESIAN_POINT('Ctrl Pts',(-20.6417807486555,24.9383902701016,0.274730862600814));
#41614=CARTESIAN_POINT('Ctrl Pts',(-20.6435554546391,24.9421025938466,0.274982975525235));
#41615=CARTESIAN_POINT('Ctrl Pts',(-20.6467863810607,24.9488279044599,0.275440577840088));
#41616=CARTESIAN_POINT('Ctrl Pts',(-20.6482401962958,24.9518420458677,0.275645983172878));
#41617=CARTESIAN_POINT('Ctrl Pts',(-20.6511570429987,24.957865442273,0.276057099041058));
#41618=CARTESIAN_POINT('Ctrl Pts',(-20.652620071659,24.960874694082,0.276262809289172));
#41619=CARTESIAN_POINT('Ctrl Pts',(-20.6567526735091,24.969341338997,0.276842485850519));
#41620=CARTESIAN_POINT('Ctrl Pts',(-20.6594329855526,24.9747934483287,0.27721682748922));
#41621=CARTESIAN_POINT('Ctrl Pts',(-20.6705372695402,24.9972206337698,0.278761068367342));
#41622=CARTESIAN_POINT('Ctrl Pts',(-20.6790953356128,25.0141285545181,0.27993566558761));
#41623=CARTESIAN_POINT('Ctrl Pts',(-20.6911030736317,25.0373414879111,0.281562901125425));
#41624=CARTESIAN_POINT('Ctrl Pts',(-20.6944255820869,25.0437121460754,0.282011018027436));
#41625=CARTESIAN_POINT('Ctrl Pts',(-20.7044612436974,25.0627988190192,0.283358216254511));
#41626=CARTESIAN_POINT('Ctrl Pts',(-20.7112381572836,25.0754809399052,0.284259547560253));
#41627=CARTESIAN_POINT('Ctrl Pts',(-20.719204133787,25.0901511934884,0.285309445986835));
#41628=CARTESIAN_POINT('Ctrl Pts',(-20.7203108284034,25.092184072269,0.285455094756321));
#41629=CARTESIAN_POINT('Ctrl Pts',(-20.7238532406541,25.0986744419272,0.2859206283418));
#41630=CARTESIAN_POINT('Ctrl Pts',(-20.7262972982619,25.103127350724,0.286240807177686));
#41631=CARTESIAN_POINT('Ctrl Pts',(-20.7321100284138,25.113658649298,0.286999909910334));
#41632=CARTESIAN_POINT('Ctrl Pts',(-20.7354878445116,25.1197319396299,0.287439154692371));
#41633=CARTESIAN_POINT('Ctrl Pts',(-20.7418796005154,25.1311372701268,0.28826682733365));
#41634=CARTESIAN_POINT('Ctrl Pts',(-20.7448891532083,25.136471744354,0.288655099824032));
#41635=CARTESIAN_POINT('Ctrl Pts',(-20.7499259767119,25.1453404127158,0.289302541225746));
#41636=CARTESIAN_POINT('Ctrl Pts',(-20.7519447846058,25.1488794159496,0.289561413777675));
#41637=CARTESIAN_POINT('Ctrl Pts',(-20.7564365919346,25.1567190481306,0.290136012669184));
#41638=CARTESIAN_POINT('Ctrl Pts',(-20.7589128179452,25.1610178081071,0.290451850837234));
#41639=CARTESIAN_POINT('Ctrl Pts',(-20.7714489344203,25.1826649484732,0.292046171275604));
#41640=CARTESIAN_POINT('Ctrl Pts',(-20.7816605028035,25.1999245839127,0.293329891275744));
#41641=CARTESIAN_POINT('Ctrl Pts',(-20.8055798534322,25.239505489108,0.296302926832801));
#41642=CARTESIAN_POINT('Ctrl Pts',(-20.8193998910517,25.2617569750201,0.297995974332773));
#41643=CARTESIAN_POINT('Ctrl Pts',(-20.8955398283283,25.3810786335741,0.30719232082289));
#41644=CARTESIAN_POINT('Ctrl Pts',(-20.9627611090807,25.4749103588654,0.314853590863943));
#41645=CARTESIAN_POINT('Ctrl Pts',(-21.2084208314198,25.7816245542864,0.341270196479512));
#41646=CARTESIAN_POINT('Ctrl Pts',(-21.4092594525579,25.9749924677834,0.360456044878661));
#41647=CARTESIAN_POINT('Ctrl Pts',(-21.6385145789546,26.1447531278,0.378429061316228));
#41648=CARTESIAN_POINT('Ctrl Pts',(-21.6446395005714,26.149255094502,0.378906580565882));
#41649=CARTESIAN_POINT('Ctrl Pts',(-21.6539485260691,26.1560468560446,0.379628250289522));
#41650=CARTESIAN_POINT('Ctrl Pts',(-21.6571209232754,26.158352540543,0.379873469358838));
#41651=CARTESIAN_POINT('Ctrl Pts',(-21.6622894954946,26.1620946372302,0.380271812759372));
#41652=CARTESIAN_POINT('Ctrl Pts',(-21.6642831080575,26.1635345569476,0.380425177380249));
#41653=CARTESIAN_POINT('Ctrl Pts',(-21.6680851947827,26.1662740602382,0.380717121035346));
#41654=CARTESIAN_POINT('Ctrl Pts',(-21.6698933701589,26.1675740529527,0.38085572839394));
#41655=CARTESIAN_POINT('Ctrl Pts',(-21.6731917108961,26.1699402220138,0.381108138079332));
#41656=CARTESIAN_POINT('Ctrl Pts',(-21.6746814353009,26.1710069998236,0.381221982272932));
#41657=CARTESIAN_POINT('Ctrl Pts',(-21.677681587593,26.173151512718,0.381450932897352));
#41658=CARTESIAN_POINT('Ctrl Pts',(-21.6791920308051,26.1742292098303,0.381566036686877));
#41659=CARTESIAN_POINT('Ctrl Pts',(-21.6834303325868,26.177247706279,0.381888564477951));
#41660=CARTESIAN_POINT('Ctrl Pts',(-21.6861602959656,26.1791855676064,0.382095784304771));
#41661=CARTESIAN_POINT('Ctrl Pts',(-21.6972923874487,26.1870616115606,0.382938655939312));
#41662=CARTESIAN_POINT('Ctrl Pts',(-21.7057200294066,26.1929638807847,0.383571853837511));
#41663=CARTESIAN_POINT('Ctrl Pts',(-21.8296205257403,26.2788557104618,0.392811592072697));
#41664=CARTESIAN_POINT('Ctrl Pts',(-21.9501656510622,26.3512461824876,0.400924583803991));
#41665=CARTESIAN_POINT('Ctrl Pts',(-22.0750360367128,26.4155367855571,0.408876748608877));
#41666=CARTESIAN_POINT('Origin',(-23.5502525316942,23.5502525316942,-77.3107734492734));
#41667=CARTESIAN_POINT('',(-22.0750357750288,26.4155366508268,1.90417269213726));
#41668=CARTESIAN_POINT('',(-22.0750360931093,26.4155368145933,1.65435918102699));
#41669=CARTESIAN_POINT('',(-22.0750360153461,26.4155367745563,-77.3107734492734));
#41670=CARTESIAN_POINT('',(-26.7730025181246,23.5505482728461,1.06385144282923));
#41671=CARTESIAN_POINT('Ctrl Pts',(-22.075035775028,26.4155366508264,1.90417269213721));
#41672=CARTESIAN_POINT('Ctrl Pts',(-21.8814507610379,26.3158677019181,1.8919715089247));
#41673=CARTESIAN_POINT('Ctrl Pts',(-21.6981541108952,26.1966789059609,1.87955594100593));
#41674=CARTESIAN_POINT('Ctrl Pts',(-21.5122014721954,26.0468261874996,1.86511320621351));
#41675=CARTESIAN_POINT('Ctrl Pts',(-21.4964692496334,26.0339003208803,1.8638759470571));
#41676=CARTESIAN_POINT('Ctrl Pts',(-21.4761651150797,26.0168932576151,1.86225858208589));
#41677=CARTESIAN_POINT('Ctrl Pts',(-21.4714806371493,26.0129466848854,1.86188399032297));
#41678=CARTESIAN_POINT('Ctrl Pts',(-21.463917553353,26.0065379933014,1.86127686259327));
#41679=CARTESIAN_POINT('Ctrl Pts',(-21.4610319717169,26.0040840993301,1.86104466549418));
#41680=CARTESIAN_POINT('Ctrl Pts',(-21.4556518048291,25.9994924445066,1.86061068984257));
#41681=CARTESIAN_POINT('Ctrl Pts',(-21.4531561468159,25.9973559434649,1.86040896351885));
#41682=CARTESIAN_POINT('Ctrl Pts',(-21.447572670071,25.9925611860239,1.85995669852832));
#41683=CARTESIAN_POINT('Ctrl Pts',(-21.4444866208581,25.9899008858646,1.85970607529586));
#41684=CARTESIAN_POINT('Ctrl Pts',(-21.4380733653824,25.9843511638366,1.85918388171023));
#41685=CARTESIAN_POINT('Ctrl Pts',(-21.4347470258812,25.9814607572817,1.85891227063435));
#41686=CARTESIAN_POINT('Ctrl Pts',(-21.4161600473663,25.9652426653331,1.85739024326999));
#41687=CARTESIAN_POINT('Ctrl Pts',(-21.4010197058138,25.9517783606637,1.85613412387737));
#41688=CARTESIAN_POINT('Ctrl Pts',(-21.2469753545308,25.8121632478877,1.84318277879368));
#41689=CARTESIAN_POINT('Ctrl Pts',(-21.1192386756393,25.6742759132547,1.83096877135852));
#41690=CARTESIAN_POINT('Ctrl Pts',(-20.8458520919125,25.3219956789153,1.80114358394728));
#41691=CARTESIAN_POINT('Ctrl Pts',(-20.7125860196738,25.099608836659,1.78330301144837));
#41692=CARTESIAN_POINT('Ctrl Pts',(-20.6058403763807,24.8604309288844,1.76631614551117));
#41693=CARTESIAN_POINT('Ctrl Pts',(-20.6043871161431,24.857160074906,1.76608425334781));
#41694=CARTESIAN_POINT('Ctrl Pts',(-20.6024120347641,24.852694724728,1.76576824097735));
#41695=CARTESIAN_POINT('Ctrl Pts',(-20.6018854903421,24.8515023351585,1.76568391062095));
#41696=CARTESIAN_POINT('Ctrl Pts',(-20.6002536604032,24.8478008887473,1.76542230129149));
#41697=CARTESIAN_POINT('Ctrl Pts',(-20.5991508502565,24.8452907339985,1.7652451334981));
#41698=CARTESIAN_POINT('Ctrl Pts',(-20.5972386254719,24.8409231083533,1.76493729225028));
#41699=CARTESIAN_POINT('Ctrl Pts',(-20.5964277584337,24.8390662795687,1.76480655250562));
#41700=CARTESIAN_POINT('Ctrl Pts',(-20.5943047766906,24.8341922721651,1.76446372681533));
#41701=CARTESIAN_POINT('Ctrl Pts',(-20.5929955268357,24.8311738387499,1.76425177353868));
#41702=CARTESIAN_POINT('Ctrl Pts',(-20.576412066822,24.7927802590375,1.76156035885763));
#41703=CARTESIAN_POINT('Ctrl Pts',(-20.5617679947572,24.7571339532501,1.75911076528892));
#41704=CARTESIAN_POINT('Ctrl Pts',(-20.5460418529123,24.7168108355699,1.75640155238525));
#41705=CARTESIAN_POINT('Ctrl Pts',(-20.5443274696509,24.7123861732833,1.75610509825657));
#41706=CARTESIAN_POINT('Ctrl Pts',(-20.5417594905385,24.70571475956,1.75565937520567));
#41707=CARTESIAN_POINT('Ctrl Pts',(-20.5408986347578,24.7034708379108,1.75550967192108));
#41708=CARTESIAN_POINT('Ctrl Pts',(-20.5394115644337,24.6995816105483,1.75525057717783));
#41709=CARTESIAN_POINT('Ctrl Pts',(-20.5387841879807,24.6979367550237,1.75514111539304));
#41710=CARTESIAN_POINT('Ctrl Pts',(-20.5374793221104,24.694507221071,1.75491313012427));
#41711=CARTESIAN_POINT('Ctrl Pts',(-20.5368020712802,24.6927224565483,1.7547946215952));
#41712=CARTESIAN_POINT('Ctrl Pts',(-20.535195681804,24.6884777593945,1.75451309751388));
#41713=CARTESIAN_POINT('Ctrl Pts',(-20.5342679646048,24.6860172820893,1.75435016813333));
#41714=CARTESIAN_POINT('Ctrl Pts',(-20.5311774994348,24.6777903101593,1.75380624468434));
#41715=CARTESIAN_POINT('Ctrl Pts',(-20.5290282527285,24.6720187060592,1.75342605999938));
#41716=CARTESIAN_POINT('Ctrl Pts',(-20.4677757133275,24.5060776487926,1.74253454572671));
#41717=CARTESIAN_POINT('Ctrl Pts',(-20.4214664321042,24.3414423300494,1.73277286198874));
#41718=CARTESIAN_POINT('Ctrl Pts',(-20.3452950612736,23.9552540009159,1.71062918018383));
#41719=CARTESIAN_POINT('Ctrl Pts',(-20.3249662010619,23.7327463799608,1.69838271240373));
#41720=CARTESIAN_POINT('Ctrl Pts',(-20.3291912901761,23.3951501879122,1.67885833496819));
#41721=CARTESIAN_POINT('Ctrl Pts',(-20.3367579337698,23.280548728671,1.67207509539306));
#41722=CARTESIAN_POINT('Ctrl Pts',(-20.3516766017234,23.1561191942171,1.6644491936628));
#41723=CARTESIAN_POINT('Ctrl Pts',(-20.3529851675831,23.1456410319546,1.66380502193365));
#41724=CARTESIAN_POINT('Ctrl Pts',(-20.3548969320148,23.1309215113061,1.66289723313203));
#41725=CARTESIAN_POINT('Ctrl Pts',(-20.3554571373852,23.1266745562569,1.66263497699177));
#41726=CARTESIAN_POINT('Ctrl Pts',(-20.3564446141178,23.1193018371944,1.66217911177237));
#41727=CARTESIAN_POINT('Ctrl Pts',(-20.3568680118607,23.1161755525261,1.66198562556488));
#41728=CARTESIAN_POINT('Ctrl Pts',(-20.357749867041,23.1097352315521,1.66158665232587));
#41729=CARTESIAN_POINT('Ctrl Pts',(-20.3582088956451,23.1064212788867,1.66138114743954));
#41730=CARTESIAN_POINT('Ctrl Pts',(-20.3592962241687,23.0986602630068,1.66089938134118));
#41731=CARTESIAN_POINT('Ctrl Pts',(-20.3599286603854,23.0942137948462,1.66062298928055));
#41732=CARTESIAN_POINT('Ctrl Pts',(-20.3612833380543,23.0848302058941,1.66003890452354));
#41733=CARTESIAN_POINT('Ctrl Pts',(-20.3620077542829,23.0798934154878,1.65973114338011));
#41734=CARTESIAN_POINT('Ctrl Pts',(-20.3673481281932,23.0440787768531,1.6574950172375));
#41735=CARTESIAN_POINT('Ctrl Pts',(-20.372400973753,23.0132686613625,1.6555528195199));
#41736=CARTESIAN_POINT('Ctrl Pts',(-20.3879687546237,22.9262769612286,1.65001452872419));
#41737=CARTESIAN_POINT('Ctrl Pts',(-20.3995313101981,22.8702971542423,1.64638565805902));
#41738=CARTESIAN_POINT('Ctrl Pts',(-20.4284850469749,22.7467952008307,1.6382312942406));
#41739=CARTESIAN_POINT('Ctrl Pts',(-20.4465909700144,22.6794714247532,1.63368589977613));
#41740=CARTESIAN_POINT('Ctrl Pts',(-20.5163122364266,22.4501523903064,1.61786948749574));
#41741=CARTESIAN_POINT('Ctrl Pts',(-20.5785477202612,22.2916912918582,1.60633997128058));
#41742=CARTESIAN_POINT('Ctrl Pts',(-20.7132603561785,22.0151505136336,1.58553650438964));
#41743=CARTESIAN_POINT('Ctrl Pts',(-20.7814095078298,21.8953877412622,1.57627711316599));
#41744=CARTESIAN_POINT('Ctrl Pts',(-20.8620392211563,21.7726950825497,1.56676387830214));
#41745=CARTESIAN_POINT('Ctrl Pts',(-20.8670970243253,21.7650696796998,1.56617253624986));
#41746=CARTESIAN_POINT('Ctrl Pts',(-20.8774591246889,21.7495907714466,1.56497214009515));
#41747=CARTESIAN_POINT('Ctrl Pts',(-20.8827657330968,21.7417389002452,1.5643632119043));
#41748=CARTESIAN_POINT('Ctrl Pts',(-20.8911207591429,21.7294932468399,1.56341365778343));
#41749=CARTESIAN_POINT('Ctrl Pts',(-20.8941455649354,21.7250835150961,1.56307174240534));
#41750=CARTESIAN_POINT('Ctrl Pts',(-20.8999617137211,21.7166494861608,1.56241787521868));
#41751=CARTESIAN_POINT('Ctrl Pts',(-20.9027512799573,21.7126239862143,1.56210582356671));
#41752=CARTESIAN_POINT('Ctrl Pts',(-20.9103929869869,21.7016500948953,1.56125526951302));
#41753=CARTESIAN_POINT('Ctrl Pts',(-20.9152634171564,21.6947144008757,1.56071784491774));
#41754=CARTESIAN_POINT('Ctrl Pts',(-20.9220532448787,21.6851260507455,1.55997516066795));
#41755=CARTESIAN_POINT('Ctrl Pts',(-20.9239493597191,21.6824570583518,1.55976845957951));
#41756=CARTESIAN_POINT('Ctrl Pts',(-20.9328870110855,21.6699168388114,1.5587974409993));
#41757=CARTESIAN_POINT('Ctrl Pts',(-20.9399802782132,21.6600823382348,1.55803640910593));
#41758=CARTESIAN_POINT('Ctrl Pts',(-20.9492348983139,21.6474026708905,1.55705607774178));
#41759=CARTESIAN_POINT('Ctrl Pts',(-20.951345589253,21.6445209066374,1.55683333209414));
#41760=CARTESIAN_POINT('Ctrl Pts',(-20.9545866981573,21.6401111611257,1.5564925788639));
#41761=CARTESIAN_POINT('Ctrl Pts',(-20.955713675064,21.6385806727111,1.55637433184176));
#41762=CARTESIAN_POINT('Ctrl Pts',(-20.9579379101103,21.6355656452746,1.55614142498344));
#41763=CARTESIAN_POINT('Ctrl Pts',(-20.9590350841611,21.6340810597374,1.55602676070396));
#41764=CARTESIAN_POINT('Ctrl Pts',(-20.9614807411735,21.6307777845123,1.55577166664929));
#41765=CARTESIAN_POINT('Ctrl Pts',(-20.96282986209,21.6289595771038,1.55563128281289));
#41766=CARTESIAN_POINT('Ctrl Pts',(-20.966728204985,21.6237173417172,1.55522660132314));
#41767=CARTESIAN_POINT('Ctrl Pts',(-20.9692823278778,21.6202969383116,1.55496264694418));
#41768=CARTESIAN_POINT('Ctrl Pts',(-20.9864669412194,21.5973789531396,1.55319457193935));
#41769=CARTESIAN_POINT('Ctrl Pts',(-21.001311956288,21.5780421482168,1.55170529973201));
#41770=CARTESIAN_POINT('Ctrl Pts',(-21.0479167378743,21.5187410956292,1.54713949584041));
#41771=CARTESIAN_POINT('Ctrl Pts',(-21.0804089892362,21.4793598148726,1.54410938244089));
#41772=CARTESIAN_POINT('Ctrl Pts',(-21.1534790869431,21.3949649195445,1.53757872223916));
#41773=CARTESIAN_POINT('Ctrl Pts',(-21.1944186306777,21.3502900405086,1.53409724814066));
#41774=CARTESIAN_POINT('Ctrl Pts',(-21.2637108287791,21.2788296594606,1.52843695567045));
#41775=CARTESIAN_POINT('Ctrl Pts',(-21.2913318337374,21.2513588386409,1.52623742004462));
#41776=CARTESIAN_POINT('Ctrl Pts',(-21.3431828940148,21.2016267456452,1.52219691617058));
#41777=CARTESIAN_POINT('Ctrl Pts',(-21.3672686580242,21.1792230272889,1.52035366086074));
#41778=CARTESIAN_POINT('Ctrl Pts',(-21.5432873739169,21.0204527926601,1.50709023911515));
#41779=CARTESIAN_POINT('Ctrl Pts',(-21.7075195564533,20.8984372305199,1.49577043300807));
#41780=CARTESIAN_POINT('Ctrl Pts',(-21.9674779889894,20.7411815979433,1.4780917613915));
#41781=CARTESIAN_POINT('Ctrl Pts',(-22.0551119110054,20.6935750583475,1.47217486568356));
#41782=CARTESIAN_POINT('Ctrl Pts',(-22.1539876527791,20.645658569912,1.46548719573802));
#41783=CARTESIAN_POINT('Ctrl Pts',(-22.1631916807759,20.6412520354758,1.46486457902553));
#41784=CARTESIAN_POINT('Ctrl Pts',(-22.176232426546,20.6350845893119,1.46398225281223));
#41785=CARTESIAN_POINT('Ctrl Pts',(-22.180051981342,20.6332873565192,1.46372380430496));
#41786=CARTESIAN_POINT('Ctrl Pts',(-22.1867180047453,20.6301667435638,1.46327271056255));
#41787=CARTESIAN_POINT('Ctrl Pts',(-22.1895629030109,20.6288400051053,1.46308018188672));
#41788=CARTESIAN_POINT('Ctrl Pts',(-22.1954541529114,20.6261030511894,1.46268146277393));
#41789=CARTESIAN_POINT('Ctrl Pts',(-22.1985007771107,20.6246934354981,1.46247525192044));
#41790=CARTESIAN_POINT('Ctrl Pts',(-22.2056951763517,20.6213783596693,1.46198825902148));
#41791=CARTESIAN_POINT('Ctrl Pts',(-22.209844799986,20.6194769500786,1.46170733754462));
#41792=CARTESIAN_POINT('Ctrl Pts',(-22.218626204959,20.6154757512555,1.46111278165286));
#41793=CARTESIAN_POINT('Ctrl Pts',(-22.2232589410106,20.6133780987526,1.46079907440684));
#41794=CARTESIAN_POINT('Ctrl Pts',(-22.2584688064079,20.5975357746459,1.45841447894258));
#41795=CARTESIAN_POINT('Ctrl Pts',(-22.2892528096187,20.5842584311879,1.45632760418596));
#41796=CARTESIAN_POINT('Ctrl Pts',(-22.3783400248555,20.5474721256919,1.45028011420247));
#41797=CARTESIAN_POINT('Ctrl Pts',(-22.4371286079786,20.5251866917094,1.44627913062091));
#41798=CARTESIAN_POINT('Ctrl Pts',(-22.570739136822,20.4789600368383,1.43715935687858));
#41799=CARTESIAN_POINT('Ctrl Pts',(-22.6458589165091,20.4560071030729,1.43201331010333));
#41800=CARTESIAN_POINT('Ctrl Pts',(-22.9999474985609,20.361810859115,1.40770625984286));
#41801=CARTESIAN_POINT('Ctrl Pts',(-23.2867946499104,20.3254157043369,1.38772806999562));
#41802=CARTESIAN_POINT('Ctrl Pts',(-23.6268156828161,20.327989796836,1.36565773507302));
#41803=CARTESIAN_POINT('Ctrl Pts',(-23.6789686312704,20.3296513459005,1.36232180446997));
#41804=CARTESIAN_POINT('Ctrl Pts',(-23.7367816849261,20.3329000086425,1.35869523291549));
#41805=CARTESIAN_POINT('Ctrl Pts',(-23.742500729226,20.3332366762247,1.35833725885135));
#41806=CARTESIAN_POINT('Ctrl Pts',(-23.750512584493,20.3337297578467,1.35783688848985));
#41807=CARTESIAN_POINT('Ctrl Pts',(-23.7528061285321,20.3338733743318,1.35769377652903));
#41808=CARTESIAN_POINT('Ctrl Pts',(-23.7570030923822,20.3341406856257,1.35743213300354));
#41809=CARTESIAN_POINT('Ctrl Pts',(-23.7589065585771,20.3342636172402,1.35731355817461));
#41810=CARTESIAN_POINT('Ctrl Pts',(-23.7627733705782,20.3345167951644,1.35707286158511));
#41811=CARTESIAN_POINT('Ctrl Pts',(-23.7647367067801,20.3346471496794,1.35695074611826));
#41812=CARTESIAN_POINT('Ctrl Pts',(-23.7696165315406,20.3349756317696,1.35664746669998));
#41813=CARTESIAN_POINT('Ctrl Pts',(-23.7725328797192,20.3351759300156,1.35646642590578));
#41814=CARTESIAN_POINT('Ctrl Pts',(-23.783439876142,20.3359399468842,1.35579011161252));
#41815=CARTESIAN_POINT('Ctrl Pts',(-23.7914287730758,20.3365294953536,1.35529628550864));
#41816=CARTESIAN_POINT('Ctrl Pts',(-23.9291236107938,20.3472071628721,1.34681016849553));
#41817=CARTESIAN_POINT('Ctrl Pts',(-24.0581221247887,20.365111936138,1.33924647735657));
#41818=CARTESIAN_POINT('Ctrl Pts',(-24.2610421145562,20.4059240283525,1.32747436309305));
#41819=CARTESIAN_POINT('Ctrl Pts',(-24.335819967173,20.4237676003324,1.32316439338793));
#41820=CARTESIAN_POINT('Ctrl Pts',(-24.5086141231305,20.4715915209475,1.31313662367713));
#41821=CARTESIAN_POINT('Ctrl Pts',(-24.6059784341575,20.5036063466133,1.30743245864895));
#41822=CARTESIAN_POINT('Ctrl Pts',(-24.8831883201678,20.6096441688844,1.29069761408952));
#41823=CARTESIAN_POINT('Ctrl Pts',(-25.0580425704263,20.6953537032487,1.27949016491133));
#41824=CARTESIAN_POINT('Ctrl Pts',(-25.23428174683,20.8024706633733,1.26695209025099));
#41825=CARTESIAN_POINT('Ctrl Pts',(-25.2444313590026,20.8087168874943,1.2662255210112));
#41826=CARTESIAN_POINT('Ctrl Pts',(-25.2583750474245,20.817405044599,1.26522103824138));
#41827=CARTESIAN_POINT('Ctrl Pts',(-25.2621990788703,20.8197989181453,1.26494490235496));
#41828=CARTESIAN_POINT('Ctrl Pts',(-25.2687393142346,20.8239122970226,1.26447149343682));
#41829=CARTESIAN_POINT('Ctrl Pts',(-25.2714580029765,20.8256278561708,1.26427436696575));
#41830=CARTESIAN_POINT('Ctrl Pts',(-25.2769726524914,20.8291192828331,1.26387382477098));
#41831=CARTESIAN_POINT('Ctrl Pts',(-25.2797684505113,20.8308953980956,1.26367040001719));
#41832=CARTESIAN_POINT('Ctrl Pts',(-25.286182069086,20.8349837349184,1.26320291106151));
#41833=CARTESIAN_POINT('Ctrl Pts',(-25.289798010987,20.8372988788058,1.26293873812384));
#41834=CARTESIAN_POINT('Ctrl Pts',(-25.2973708452006,20.8421688281909,1.2623842041558));
#41835=CARTESIAN_POINT('Ctrl Pts',(-25.3013267821481,20.8447250940976,1.26209378887469));
#41836=CARTESIAN_POINT('Ctrl Pts',(-25.3265746622469,20.8611184584719,1.26023555565196));
#41837=CARTESIAN_POINT('Ctrl Pts',(-25.3477075482556,20.8751978071666,1.25865866422172));
#41838=CARTESIAN_POINT('Ctrl Pts',(-25.5800973033549,21.0340197534594,1.24107349919458));
#41839=CARTESIAN_POINT('Ctrl Pts',(-25.7735026921135,21.2031686147822,1.22406272097569));
#41840=CARTESIAN_POINT('Ctrl Pts',(-26.0747637857122,21.5376283685949,1.19361314385912));
#41841=CARTESIAN_POINT('Ctrl Pts',(-26.1914122081893,21.6933464045357,1.18039870522529));
#41842=CARTESIAN_POINT('Ctrl Pts',(-26.2965595046832,21.8638500858632,1.16748648705273));
#41843=CARTESIAN_POINT('Ctrl Pts',(-26.2997648147177,21.8690810931143,1.16709178879035));
#41844=CARTESIAN_POINT('Ctrl Pts',(-26.3212638904364,21.9043931396477,1.16443725254659));
#41845=CARTESIAN_POINT('Ctrl Pts',(-26.3390795319283,21.9347645851838,1.16220232572372));
#41846=CARTESIAN_POINT('Ctrl Pts',(-26.3586680483521,21.9694485533358,1.15970936419581));
#41847=CARTESIAN_POINT('Ctrl Pts',(-26.3609326930063,21.973478621573,1.1594205925036));
#41848=CARTESIAN_POINT('Ctrl Pts',(-26.3643462417632,21.9795839543467,1.15898448882889));
#41849=CARTESIAN_POINT('Ctrl Pts',(-26.3655015268214,21.9816556158356,1.15883674816047));
#41850=CARTESIAN_POINT('Ctrl Pts',(-26.3675063490557,21.9852600198799,1.15858011603939));
#41851=CARTESIAN_POINT('Ctrl Pts',(-26.3683569231326,21.9867921796346,1.15847115743749));
#41852=CARTESIAN_POINT('Ctrl Pts',(-26.3701346428063,21.9900005932772,1.15824326745465));
#41853=CARTESIAN_POINT('Ctrl Pts',(-26.3710615430849,21.9916769790876,1.15812435237936));
#41854=CARTESIAN_POINT('Ctrl Pts',(-26.3732747217799,21.9956881610281,1.15784018993199));
#41855=CARTESIAN_POINT('Ctrl Pts',(-26.3745596029461,21.9980237355239,1.15767503309625));
#41856=CARTESIAN_POINT('Ctrl Pts',(-26.3789041702153,22.0059442646638,1.15711595517815));
#41857=CARTESIAN_POINT('Ctrl Pts',(-26.3819502252139,22.0115367392623,1.15672290662291));
#41858=CARTESIAN_POINT('Ctrl Pts',(-26.3891497823511,22.0248487152359,1.15579126720568));
#41859=CARTESIAN_POINT('Ctrl Pts',(-26.393288430092,22.032576252782,1.15525359819272));
#41860=CARTESIAN_POINT('Ctrl Pts',(-26.441583725735,22.1236423588657,1.14895311202748));
#41861=CARTESIAN_POINT('Ctrl Pts',(-26.4820977764742,22.2088726929073,1.14340705688869));
#41862=CARTESIAN_POINT('Ctrl Pts',(-26.6203476069523,22.5360214612851,1.1229624250592));
#41863=CARTESIAN_POINT('Ctrl Pts',(-26.692339172238,22.7877199375945,1.10883621379078));
#41864=CARTESIAN_POINT('Ctrl Pts',(-26.7549740880502,23.182581709233,1.08596053099294));
#41865=CARTESIAN_POINT('Ctrl Pts',(-26.7678420929857,23.3210539961626,1.0778252309071));
#41866=CARTESIAN_POINT('Ctrl Pts',(-26.7721376785587,23.4742334600604,1.06852386079418));
#41867=CARTESIAN_POINT('Ctrl Pts',(-26.7724437667979,23.4885562361089,1.06765134792028));
#41868=CARTESIAN_POINT('Ctrl Pts',(-26.7727339722753,23.5082969273394,1.06644477344609));
#41869=CARTESIAN_POINT('Ctrl Pts',(-26.7727999425391,23.5137136220729,1.06611328235863));
#41870=CARTESIAN_POINT('Ctrl Pts',(-26.7728832979791,23.5223448267491,1.06558439774986));
#41871=CARTESIAN_POINT('Ctrl Pts',(-26.7729095314212,23.5255592574914,1.0653872822359));
#41872=CARTESIAN_POINT('Ctrl Pts',(-26.7729525099123,23.5320077431331,1.06499154783542));
#41873=CARTESIAN_POINT('Ctrl Pts',(-26.7729691961829,23.5352417947467,1.06479292732375));
#41874=CARTESIAN_POINT('Ctrl Pts',(-26.7729933534064,23.5418525038813,1.06438661654675));
#41875=CARTESIAN_POINT('Ctrl Pts',(-26.7730003856187,23.5452291579355,1.06417891275826));
#41876=CARTESIAN_POINT('Ctrl Pts',(-26.7730024418284,23.5492532957307,1.06393118172865));
#41877=CARTESIAN_POINT('Ctrl Pts',(-26.7730025775425,23.5499007845161,1.06389131534507));
#41878=CARTESIAN_POINT('Ctrl Pts',(-26.7730025181246,23.5505482728461,1.06385144282923));
#41879=CARTESIAN_POINT('Ctrl Pts',(-26.7730025181501,23.5505479950934,1.06385145993333));
#41880=CARTESIAN_POINT('Ctrl Pts',(-26.7730022618683,23.5533433743501,1.0636793196899));
#41881=CARTESIAN_POINT('Ctrl Pts',(-26.7729983685636,23.5561387455046,1.06350706512355));
#41882=CARTESIAN_POINT('Ctrl Pts',(-26.772952457919,23.5731815149597,1.06245616260223));
#41883=CARTESIAN_POINT('Ctrl Pts',(-26.7728195988542,23.5874283294327,1.06157466572968));
#41884=CARTESIAN_POINT('Ctrl Pts',(-26.7695656810077,23.7913374756817,1.04891409998377));
#41885=CARTESIAN_POINT('Ctrl Pts',(-26.7498010758502,23.9803281996212,1.03660008540109));
#41886=CARTESIAN_POINT('Ctrl Pts',(-26.674593879202,24.366405226574,1.01032532656749));
#41887=CARTESIAN_POINT('Ctrl Pts',(-26.6167766994715,24.5622008701433,0.99636727538878));
#41888=CARTESIAN_POINT('Ctrl Pts',(-26.5108996430848,24.8258517894404,0.977440662005678));
#41889=CARTESIAN_POINT('Ctrl Pts',(-26.4781457219519,24.8993368071326,0.972155526978332));
#41890=CARTESIAN_POINT('Ctrl Pts',(-26.4286034850465,25.0001598725442,0.964962154658452));
#41891=CARTESIAN_POINT('Ctrl Pts',(-26.4141077492004,25.0285857121237,0.96294079985228));
#41892=CARTESIAN_POINT('Ctrl Pts',(-26.3970532862464,25.0608365080325,0.960659199583425));
#41893=CARTESIAN_POINT('Ctrl Pts',(-26.3949063666697,25.0648756021193,0.960373664613543));
#41894=CARTESIAN_POINT('Ctrl Pts',(-26.3916537351577,25.0709636100479,0.959943623667648));
#41895=CARTESIAN_POINT('Ctrl Pts',(-26.39055440217,25.0730158972654,0.959798713481767));
#41896=CARTESIAN_POINT('Ctrl Pts',(-26.3885775133581,25.0766968587514,0.959538910703062));
#41897=CARTESIAN_POINT('Ctrl Pts',(-26.3877007810336,25.0783259649825,0.959423965848513));
#41898=CARTESIAN_POINT('Ctrl Pts',(-26.3859382456897,25.0815942850436,0.959193439022753));
#41899=CARTESIAN_POINT('Ctrl Pts',(-26.3850524273688,25.0832334792715,0.959077858737703));
#41900=CARTESIAN_POINT('Ctrl Pts',(-26.3825525971509,25.0878498034163,0.958752464831404));
#41901=CARTESIAN_POINT('Ctrl Pts',(-26.3809353074311,25.0908251700954,0.958542861443316));
#41902=CARTESIAN_POINT('Ctrl Pts',(-26.3742412343576,25.103094286924,0.957679034380685));
#41903=CARTESIAN_POINT('Ctrl Pts',(-26.3691232726928,25.1123656717967,0.957027420142438));
#41904=CARTESIAN_POINT('Ctrl Pts',(-26.2745081225734,25.2817854357539,0.945138252250335));
#41905=CARTESIAN_POINT('Ctrl Pts',(-26.1715274988144,25.4340555425234,0.934739891450258));
#41906=CARTESIAN_POINT('Ctrl Pts',(-25.9499571546216,25.7080394846369,0.914986172828499));
#41907=CARTESIAN_POINT('Ctrl Pts',(-25.8336347860798,25.8307767042791,0.905639993619675));
#41908=CARTESIAN_POINT('Ctrl Pts',(-25.6531283189693,25.9935158917294,0.891760000630903));
#41909=CARTESIAN_POINT('Ctrl Pts',(-25.5963265305947,26.0412769358294,0.887472353013706));
#41910=CARTESIAN_POINT('Ctrl Pts',(-25.4822596851849,26.1306532324259,0.878956564732244));
#41911=CARTESIAN_POINT('Ctrl Pts',(-25.4251723854354,26.1724260217868,0.87473743717121));
#41912=CARTESIAN_POINT('Ctrl Pts',(-25.354900121296,26.2203781473119,0.869572757252184));
#41913=CARTESIAN_POINT('Ctrl Pts',(-25.3429861090755,26.2283918178253,0.868698127091755));
#41914=CARTESIAN_POINT('Ctrl Pts',(-25.3266463597186,26.2392244644244,0.86749979684013));
#41915=CARTESIAN_POINT('Ctrl Pts',(-25.3222665754128,26.2421127278416,0.867178707798934));
#41916=CARTESIAN_POINT('Ctrl Pts',(-25.3152607099786,26.2467082617412,0.866665275473352));
#41917=CARTESIAN_POINT('Ctrl Pts',(-25.3126391457502,26.2484224292354,0.866473191222828));
#41918=CARTESIAN_POINT('Ctrl Pts',(-25.3072367924786,26.2519436443291,0.866077436164229));
#41919=CARTESIAN_POINT('Ctrl Pts',(-25.3044557055198,26.2537502264495,0.865873748228727));
#41920=CARTESIAN_POINT('Ctrl Pts',(-25.298050099156,26.2578972352053,0.865404696401294));
#41921=CARTESIAN_POINT('Ctrl Pts',(-25.2944236645493,26.2602346785548,0.865139221544065));
#41922=CARTESIAN_POINT('Ctrl Pts',(-25.2833818583141,26.2673204060378,0.864331110844406));
#41923=CARTESIAN_POINT('Ctrl Pts',(-25.2759517562986,26.272045558416,0.863787615058523));
#41924=CARTESIAN_POINT('Ctrl Pts',(-25.2192692615357,26.3077672284368,0.859643446730582));
#41925=CARTESIAN_POINT('Ctrl Pts',(-25.1692075360091,26.3374533006186,0.855994675877741));
#41926=CARTESIAN_POINT('Ctrl Pts',(-24.8517879203346,26.5142423148024,0.832907658370451));
#41927=CARTESIAN_POINT('Ctrl Pts',(-24.5655039130546,26.6240806033784,0.812081688067338));
#41928=CARTESIAN_POINT('Ctrl Pts',(-24.1237873074547,26.7250129503782,0.781595007996346));
#41929=CARTESIAN_POINT('Ctrl Pts',(-23.9773026401792,26.7480152345837,0.771778741118466));
#41930=CARTESIAN_POINT('Ctrl Pts',(-23.8236508809171,26.7613906835773,0.762114737343932));
#41931=CARTESIAN_POINT('Ctrl Pts',(-23.8175628977816,26.7619032065772,0.761732867924659));
#41932=CARTESIAN_POINT('Ctrl Pts',(-23.8088611205264,26.7626108600255,0.761188565604464));
#41933=CARTESIAN_POINT('Ctrl Pts',(-23.8062485368686,26.7628201149941,0.761025342050356));
#41934=CARTESIAN_POINT('Ctrl Pts',(-23.8017342101189,26.7631761482825,0.760743646345505));
#41935=CARTESIAN_POINT('Ctrl Pts',(-23.7998325894122,26.7633244256108,0.760625089030307));
#41936=CARTESIAN_POINT('Ctrl Pts',(-23.7961735838451,26.7636064656487,0.760397169277749));
#41937=CARTESIAN_POINT('Ctrl Pts',(-23.7944162243434,26.7637404747215,0.760287792889584));
#41938=CARTESIAN_POINT('Ctrl Pts',(-23.790254382727,26.7640544060914,0.760028974300967));
#41939=CARTESIAN_POINT('Ctrl Pts',(-23.7878498027661,26.7642330719661,0.759879603486389));
#41940=CARTESIAN_POINT('Ctrl Pts',(-23.7806818780102,26.7647575772358,0.759434826830249));
#41941=CARTESIAN_POINT('Ctrl Pts',(-23.7759179355652,26.7650955290496,0.759139864188646));
#41942=CARTESIAN_POINT('Ctrl Pts',(-23.7318307283083,26.768124573698,0.756415993953826));
#41943=CARTESIAN_POINT('Ctrl Pts',(-23.6924597871926,26.7701047893787,0.754026330346571));
#41944=CARTESIAN_POINT('Ctrl Pts',(-23.652582814233,26.7713775376484,0.751640331108725));
#41945=CARTESIAN_POINT('Ctrl Pts',(-23.6521053427244,26.7713926707744,0.751611767058734));
#41946=CARTESIAN_POINT('Ctrl Pts',(-23.647029499083,26.7715524163711,0.751308164806257));
#41947=CARTESIAN_POINT('Ctrl Pts',(-23.6424307999821,26.7716872890298,0.751033563017467));
#41948=CARTESIAN_POINT('Ctrl Pts',(-23.6333411723795,26.7719343938504,0.750491678173563));
#41949=CARTESIAN_POINT('Ctrl Pts',(-23.628850268389,26.7720470843275,0.750224375764226));
#41950=CARTESIAN_POINT('Ctrl Pts',(-23.616321233354,26.7723352635547,0.749479789619918));
#41951=CARTESIAN_POINT('Ctrl Pts',(-23.6082826095365,26.7724900643311,0.749003386789321));
#41952=CARTESIAN_POINT('Ctrl Pts',(-23.4692676032212,26.7746467067939,0.740786371494307));
#41953=CARTESIAN_POINT('Ctrl Pts',(-23.3382772669552,26.7686914472251,0.73337216273358));
#41954=CARTESIAN_POINT('Ctrl Pts',(-23.0392087468997,26.7367503371296,0.716503703248535));
#41955=CARTESIAN_POINT('Ctrl Pts',(-22.8721080548968,26.7054153622454,0.707111732053728));
#41956=CARTESIAN_POINT('Ctrl Pts',(-22.5644942953383,26.6221541235516,0.688922240850701));
#41957=CARTESIAN_POINT('Ctrl Pts',(-22.4236228484983,26.5733296306818,0.680217176689868));
#41958=CARTESIAN_POINT('Ctrl Pts',(-22.2748972972629,26.5099399508598,0.67039245023387));
#41959=CARTESIAN_POINT('Ctrl Pts',(-22.2631813460264,26.5048639018784,0.669614173759584));
#41960=CARTESIAN_POINT('Ctrl Pts',(-22.2469139320065,26.4977007709883,0.668527404569993));
#41961=CARTESIAN_POINT('Ctrl Pts',(-22.2423365931142,26.4956724552219,0.668220928177105));
#41962=CARTESIAN_POINT('Ctrl Pts',(-22.2348988213699,26.4923558645031,0.66772181646321));
#41963=CARTESIAN_POINT('Ctrl Pts',(-22.2320354982717,26.4910740592386,0.667529403823884));
#41964=CARTESIAN_POINT('Ctrl Pts',(-22.2261173419208,26.4884143366996,0.667131149791656));
#41965=CARTESIAN_POINT('Ctrl Pts',(-22.2230627779997,26.487035831624,0.666925288317764));
#41966=CARTESIAN_POINT('Ctrl Pts',(-22.2158988449067,26.4837893351799,0.66644174887494));
#41967=CARTESIAN_POINT('Ctrl Pts',(-22.2117912472008,26.4819174730593,0.666163937618385));
#41968=CARTESIAN_POINT('Ctrl Pts',(-22.1987934838375,26.475961287087,0.665283058514088));
#41969=CARTESIAN_POINT('Ctrl Pts',(-22.189918040534,26.4718451364542,0.664678891084597));
#41970=CARTESIAN_POINT('Ctrl Pts',(-22.1453991597498,26.45095184285,0.661634858846061));
#41971=CARTESIAN_POINT('Ctrl Pts',(-22.1100514947494,26.4335647989318,0.659174052746652));
#41972=CARTESIAN_POINT('Ctrl Pts',(-22.0750360011372,26.4155367672407,0.656690934610686));
#41973=CARTESIAN_POINT('Ctrl Pts',(-22.0750360367128,26.4155367855571,0.408876748608875));
#41974=CARTESIAN_POINT('Ctrl Pts',(-22.0995036376718,26.4281341425135,0.410434927469236));
#41975=CARTESIAN_POINT('Ctrl Pts',(-22.1241373073762,26.4404205190396,0.4119868098433));
#41976=CARTESIAN_POINT('Ctrl Pts',(-22.3097216831781,26.5300314085391,0.42357291862522));
#41977=CARTESIAN_POINT('Ctrl Pts',(-22.4766823563153,26.5941719314614,0.433427277109405));
#41978=CARTESIAN_POINT('Ctrl Pts',(-22.7408020895591,26.6711871429517,0.449108882320199));
#41979=CARTESIAN_POINT('Ctrl Pts',(-22.8346703305267,26.6940373028288,0.454695284139118));
#41980=CARTESIAN_POINT('Ctrl Pts',(-22.9913023769119,26.7247870842978,0.46414302470922));
#41981=CARTESIAN_POINT('Ctrl Pts',(-23.0535269468766,26.735116383894,0.467928013908913));
#41982=CARTESIAN_POINT('Ctrl Pts',(-23.1243180689114,26.7447427371464,0.472282943377488));
#41983=CARTESIAN_POINT('Ctrl Pts',(-23.1326290603348,26.7458398757349,0.472794970898169));
#41984=CARTESIAN_POINT('Ctrl Pts',(-23.1451274559382,26.7474402056085,0.473566138430657));
#41985=CARTESIAN_POINT('Ctrl Pts',(-23.1493117669356,26.7479676303426,0.473824511230317));
#41986=CARTESIAN_POINT('Ctrl Pts',(-23.1565130584911,26.7488609831649,0.474269516692919));
#41987=CARTESIAN_POINT('Ctrl Pts',(-23.1595295509132,26.7492308609055,0.474456024170555));
#41988=CARTESIAN_POINT('Ctrl Pts',(-23.165745790361,26.7499841632206,0.474840582898491));
#41989=CARTESIAN_POINT('Ctrl Pts',(-23.1689455976152,26.7503670561788,0.475038650755829));
#41990=CARTESIAN_POINT('Ctrl Pts',(-23.1766550107426,26.7512778471369,0.475516145693151));
#41991=CARTESIAN_POINT('Ctrl Pts',(-23.1811651595905,26.7518010147242,0.475795722019741));
#41992=CARTESIAN_POINT('Ctrl Pts',(-23.1950255521417,26.7533791129557,0.476655627947201));
#41993=CARTESIAN_POINT('Ctrl Pts',(-23.2043792595696,26.7544026185659,0.4772369490259));
#41994=CARTESIAN_POINT('Ctrl Pts',(-23.3145684451345,26.765971670739,0.484097249267685));
#41995=CARTESIAN_POINT('Ctrl Pts',(-23.4158326476031,26.7717931778601,0.490524737896736));
#41996=CARTESIAN_POINT('Ctrl Pts',(-23.8067120235829,26.7758029328656,0.515845359116236));
#41997=CARTESIAN_POINT('Ctrl Pts',(-24.0952899525238,26.7397403553443,0.535769536277604));
#41998=CARTESIAN_POINT('Ctrl Pts',(-24.4176120450762,26.6544012371775,0.558038621149693));
#41999=CARTESIAN_POINT('Ctrl Pts',(-24.4598928680931,26.6422755672834,0.560956341297723));
#42000=CARTESIAN_POINT('Ctrl Pts',(-24.5667552660202,26.6092467823837,0.568301523436472));
#42001=CARTESIAN_POINT('Ctrl Pts',(-24.6309533289382,26.587160663152,0.572686797668253));
#42002=CARTESIAN_POINT('Ctrl Pts',(-24.7011931172345,26.5604860709049,0.577418185681183));
#42003=CARTESIAN_POINT('Ctrl Pts',(-24.707966508835,26.5578875729754,0.577873746830789));
#42004=CARTESIAN_POINT('Ctrl Pts',(-24.7182659248607,26.5538964265036,0.57856533211947));
#42005=CARTESIAN_POINT('Ctrl Pts',(-24.7217983072182,26.5525204127538,0.578802322128006));
#42006=CARTESIAN_POINT('Ctrl Pts',(-24.7283154188769,26.5499684661719,0.579239174715101));
#42007=CARTESIAN_POINT('Ctrl Pts',(-24.7313008304196,26.548794305625,0.579439142269598));
#42008=CARTESIAN_POINT('Ctrl Pts',(-24.7361569948146,26.5468760015715,0.57976416653539));
#42009=CARTESIAN_POINT('Ctrl Pts',(-24.7380288030023,26.5461345629564,0.579889386761071));
#42010=CARTESIAN_POINT('Ctrl Pts',(-24.7416520469411,26.5446954367826,0.580131655889902));
#42011=CARTESIAN_POINT('Ctrl Pts',(-24.7434035600598,26.5439979684823,0.580248717279999));
#42012=CARTESIAN_POINT('Ctrl Pts',(-24.7474235708563,26.5423930756796,0.580517270115671));
#42013=CARTESIAN_POINT('Ctrl Pts',(-24.749691654668,26.5414846059982,0.580668697821311));
#42014=CARTESIAN_POINT('Ctrl Pts',(-24.7568623185684,26.5386029651769,0.581147168108609));
#42015=CARTESIAN_POINT('Ctrl Pts',(-24.761761111704,26.536620300838,0.581473636627261));
#42016=CARTESIAN_POINT('Ctrl Pts',(-24.8026808536453,26.5199417971001,0.584197393056457));
#42017=CARTESIAN_POINT('Ctrl Pts',(-24.8384398091579,26.5046060827787,0.586556592443559));
#42018=CARTESIAN_POINT('Ctrl Pts',(-25.0081700280381,26.4281469778153,0.597693660707304));
#42019=CARTESIAN_POINT('Ctrl Pts',(-25.1381389519207,26.3585307122643,0.606042386981039));
#42020=CARTESIAN_POINT('Ctrl Pts',(-25.3361263130104,26.2343248617678,0.619154653779421));
#42021=CARTESIAN_POINT('Ctrl Pts',(-25.4074725619995,26.1854609369353,0.6239680617356));
#42022=CARTESIAN_POINT('Ctrl Pts',(-25.5504213732254,26.0788654715814,0.633953103900781));
#42023=CARTESIAN_POINT('Ctrl Pts',(-25.6216896073023,26.020820514944,0.6391238418908));
#42024=CARTESIAN_POINT('Ctrl Pts',(-25.7524727360789,25.9046613876217,0.649129813942959));
#42025=CARTESIAN_POINT('Ctrl Pts',(-25.8124080962872,25.8471342416085,0.65394555122834));
#42026=CARTESIAN_POINT('Ctrl Pts',(-25.9154825435877,25.7402497524828,0.662724490027008));
#42027=CARTESIAN_POINT('Ctrl Pts',(-25.959464799315,25.6917697865474,0.666649754557606));
#42028=CARTESIAN_POINT('Ctrl Pts',(-26.0074243981403,25.6355571663038,0.671153732534353));
#42029=CARTESIAN_POINT('Ctrl Pts',(-26.0128848940787,25.6291057843242,0.671669953436111));
#42030=CARTESIAN_POINT('Ctrl Pts',(-26.0210409740907,25.6193924354149,0.672446188194751));
#42031=CARTESIAN_POINT('Ctrl Pts',(-26.0237556450177,25.6161464825928,0.67270541961517));
#42032=CARTESIAN_POINT('Ctrl Pts',(-26.028410298429,25.6105585512142,0.673151407204916));
#42033=CARTESIAN_POINT('Ctrl Pts',(-26.0303533780605,25.6082191501421,0.673338036627604));
#42034=CARTESIAN_POINT('Ctrl Pts',(-26.0343452702479,25.6033991849126,0.673722385412113));
#42035=CARTESIAN_POINT('Ctrl Pts',(-26.0363936849855,25.6009182965478,0.673920120699752));
#42036=CARTESIAN_POINT('Ctrl Pts',(-26.0413113669479,25.5949441654835,0.674396057980072));
#42037=CARTESIAN_POINT('Ctrl Pts',(-26.0441770003041,25.5914479516696,0.674674407098615));
#42038=CARTESIAN_POINT('Ctrl Pts',(-26.0529336179612,25.5807184798958,0.675528081317239));
#42039=CARTESIAN_POINT('Ctrl Pts',(-26.0588005205612,25.5734657115093,0.676104378391196));
#42040=CARTESIAN_POINT('Ctrl Pts',(-26.0804748243287,25.5464323478187,0.678249695638889));
#42041=CARTESIAN_POINT('Ctrl Pts',(-26.0960800955957,25.5264915517208,0.679826784206252));
#42042=CARTESIAN_POINT('Ctrl Pts',(-26.1152704033688,25.5013651707364,0.681807788966305));
#42043=CARTESIAN_POINT('Ctrl Pts',(-26.1190776862472,25.496349789456,0.682202904628665));
#42044=CARTESIAN_POINT('Ctrl Pts',(-26.1249527398742,25.4885632280032,0.682815870918273));
#42045=CARTESIAN_POINT('Ctrl Pts',(-26.1270308056451,25.4857998042177,0.683033320199309));
#42046=CARTESIAN_POINT('Ctrl Pts',(-26.1299448343687,25.4819117018769,0.683339142683186));
#42047=CARTESIAN_POINT('Ctrl Pts',(-26.1307845224279,25.4807898069154,0.683427371726358));
#42048=CARTESIAN_POINT('Ctrl Pts',(-26.1341437571173,25.4762954749178,0.683780760238077));
#42049=CARTESIAN_POINT('Ctrl Pts',(-26.1366574179843,25.4729186618021,0.684046146283691));
#42050=CARTESIAN_POINT('Ctrl Pts',(-26.1433079615744,25.4639477810893,0.684750826555741));
#42051=CARTESIAN_POINT('Ctrl Pts',(-26.1474333406327,25.458345248114,0.685190559379306));
#42052=CARTESIAN_POINT('Ctrl Pts',(-26.1560465883395,25.4465682127376,0.686114179150925));
#42053=CARTESIAN_POINT('Ctrl Pts',(-26.1605307223886,25.4403910433929,0.686598203694183));
#42054=CARTESIAN_POINT('Ctrl Pts',(-26.1673233637086,25.4309634920476,0.687336282696466));
#42055=CARTESIAN_POINT('Ctrl Pts',(-26.1696478769986,25.427724630274,0.687589738159199));
#42056=CARTESIAN_POINT('Ctrl Pts',(-26.1750790273205,25.4201274143702,0.688183989643753));
#42057=CARTESIAN_POINT('Ctrl Pts',(-26.1781808220264,25.4157656271529,0.68852496364681));
#42058=CARTESIAN_POINT('Ctrl Pts',(-26.1935339793735,25.3940615248334,0.690220634591346));
#42059=CARTESIAN_POINT('Ctrl Pts',(-26.2056243876301,25.3766064645495,0.691581171497676));
#42060=CARTESIAN_POINT('Ctrl Pts',(-26.361722927432,25.1464183602922,0.709482216385985));
#42061=CARTESIAN_POINT('Ctrl Pts',(-26.4799471212204,24.9173518388607,0.726951110880739));
#42062=CARTESIAN_POINT('Ctrl Pts',(-26.598671974789,24.5991184641266,0.749874264365667));
#42063=CARTESIAN_POINT('Ctrl Pts',(-26.6246274815847,24.5204076022534,0.755432953171279));
#42064=CARTESIAN_POINT('Ctrl Pts',(-26.6637379983157,24.3843806488808,0.764766814481929));
#42065=CARTESIAN_POINT('Ctrl Pts',(-26.6784116876,24.327544431243,0.76858738982242));
#42066=CARTESIAN_POINT('Ctrl Pts',(-26.6976514324485,24.243613416311,0.774083463749585));
#42067=CARTESIAN_POINT('Ctrl Pts',(-26.703436044812,24.2168131159379,0.77581685904736));
#42068=CARTESIAN_POINT('Ctrl Pts',(-26.7097524931961,24.1856240434316,0.777806559031801));
#42069=CARTESIAN_POINT('Ctrl Pts',(-26.7106179608429,24.1813050805759,0.778081475091815));
#42070=CARTESIAN_POINT('Ctrl Pts',(-26.7119204846962,24.1747351775414,0.778498727567766));
#42071=CARTESIAN_POINT('Ctrl Pts',(-26.7123639935446,24.1724855450559,0.778641432995534));
#42072=CARTESIAN_POINT('Ctrl Pts',(-26.7131638725067,24.1684053369344,0.778899953956846));
#42073=CARTESIAN_POINT('Ctrl Pts',(-26.7135210533841,24.1665749312589,0.779015815850281));
#42074=CARTESIAN_POINT('Ctrl Pts',(-26.7142366284006,24.1628908937182,0.779248784016214));
#42075=CARTESIAN_POINT('Ctrl Pts',(-26.7145949810986,24.1610372644572,0.779365887576553));
#42076=CARTESIAN_POINT('Ctrl Pts',(-26.7156146598695,24.1557378500577,0.779700354452553));
#42077=CARTESIAN_POINT('Ctrl Pts',(-26.7162719904694,24.1522912847455,0.77991748793278));
#42078=CARTESIAN_POINT('Ctrl Pts',(-26.719074614199,24.1374648235411,0.780849892412955));
#42079=CARTESIAN_POINT('Ctrl Pts',(-26.7211642252107,24.1260742990857,0.781562009672773));
#42080=CARTESIAN_POINT('Ctrl Pts',(-26.7561604236966,23.9293398994024,0.793792840328805));
#42081=CARTESIAN_POINT('Ctrl Pts',(-26.7728324644746,23.7414434010028,0.804433783195011));
#42082=CARTESIAN_POINT('Ctrl Pts',(-26.7732725053934,23.2504829657748,0.831934080181385));
#42083=CARTESIAN_POINT('Ctrl Pts',(-26.7309132814301,22.9493419044259,0.848652270162657));
#42084=CARTESIAN_POINT('Ctrl Pts',(-26.6421112696967,22.6409326161044,0.868084768824089));
#42085=CARTESIAN_POINT('Ctrl Pts',(-26.636892459408,22.6233722267457,0.869198780460152));
#42086=CARTESIAN_POINT('Ctrl Pts',(-26.6297679844223,22.6001272451644,0.870683773263436));
#42087=CARTESIAN_POINT('Ctrl Pts',(-26.627995696984,22.594401867919,0.871050373053453));
#42088=CARTESIAN_POINT('Ctrl Pts',(-26.6252140207211,22.5855036061092,0.871621449631648));
#42089=CARTESIAN_POINT('Ctrl Pts',(-26.6242156619745,22.5823272649716,0.871825563345842));
#42090=CARTESIAN_POINT('Ctrl Pts',(-26.6222129698167,22.5759899234901,0.872233328785831));
#42091=CARTESIAN_POINT('Ctrl Pts',(-26.6212086753772,22.5728289149443,0.87243697902277));
#42092=CARTESIAN_POINT('Ctrl Pts',(-26.6189428274349,22.5657351425572,0.87289458819865));
#42093=CARTESIAN_POINT('Ctrl Pts',(-26.6176785916271,22.5618032475742,0.873148635330487));
#42094=CARTESIAN_POINT('Ctrl Pts',(-26.61395514909,22.5502989206679,0.873893147675802));
#42095=CARTESIAN_POINT('Ctrl Pts',(-26.6114754483081,22.5427331993652,0.874384289069713));
#42096=CARTESIAN_POINT('Ctrl Pts',(-26.5929730385625,22.4869801156199,0.878014921971213));
#42097=CARTESIAN_POINT('Ctrl Pts',(-26.5758421891125,22.4391705981788,0.88119098441538));
#42098=CARTESIAN_POINT('Ctrl Pts',(-26.5159516436911,22.2836966588994,0.89173494847809));
#42099=CARTESIAN_POINT('Ctrl Pts',(-26.4685208557158,22.1779406787224,0.899255995543369));
#42100=CARTESIAN_POINT('Ctrl Pts',(-26.2732713663549,21.7987308700924,0.927493279158542));
#42101=CARTESIAN_POINT('Ctrl Pts',(-26.0918527940358,21.5445332298945,0.949145815305843));
#42102=CARTESIAN_POINT('Ctrl Pts',(-25.8512281201052,21.2934844071552,0.971502463498003));
#42103=CARTESIAN_POINT('Ctrl Pts',(-25.8251229029251,21.2671721312342,0.973856979799311));
#42104=CARTESIAN_POINT('Ctrl Pts',(-25.7948815950805,21.2377248218776,0.976498944525474));
#42105=CARTESIAN_POINT('Ctrl Pts',(-25.7911863278011,21.2341437770783,0.976820348778215));
#42106=CARTESIAN_POINT('Ctrl Pts',(-25.7857166701628,21.2288685336243,0.977293963726078));
#42107=CARTESIAN_POINT('Ctrl Pts',(-25.7839489202103,21.2271675085191,0.977446706642546));
#42108=CARTESIAN_POINT('Ctrl Pts',(-25.7808181539938,21.2241617924712,0.977716642952823));
#42109=CARTESIAN_POINT('Ctrl Pts',(-25.7794559333906,21.2228562791357,0.97783390108372));
#42110=CARTESIAN_POINT('Ctrl Pts',(-25.7766111756814,21.2201347334167,0.97807837006634));
#42111=CARTESIAN_POINT('Ctrl Pts',(-25.7751284368017,21.21871892215,0.978205563595296));
#42112=CARTESIAN_POINT('Ctrl Pts',(-25.7712570521657,21.2150293393294,0.978537070651937));
#42113=CARTESIAN_POINT('Ctrl Pts',(-25.7688662578002,21.2127578102714,0.978741208666828));
#42114=CARTESIAN_POINT('Ctrl Pts',(-25.758503261313,21.2029419963314,0.979623543181706));
#42115=CARTESIAN_POINT('Ctrl Pts',(-25.7504959106077,21.1954346797036,0.980298896795738));
#42116=CARTESIAN_POINT('Ctrl Pts',(-25.6924517009059,21.1415697042424,0.985149760794836));
#42117=CARTESIAN_POINT('Ctrl Pts',(-25.6409884315136,21.0967661943485,0.989212666162239));
#42118=CARTESIAN_POINT('Ctrl Pts',(-25.5540392370581,21.025793425754,0.99577120521706));
#42119=CARTESIAN_POINT('Ctrl Pts',(-25.5193729639377,20.9986608830158,0.998310694409467));
#42120=CARTESIAN_POINT('Ctrl Pts',(-25.2504710055561,20.796942359928,1.0175330764218));
#42121=CARTESIAN_POINT('Ctrl Pts',(-24.9940360356269,20.6542272665234,1.0332961043754));
#42122=CARTESIAN_POINT('Ctrl Pts',(-24.6301602949257,20.5122254939189,1.05603627288238));
#42123=CARTESIAN_POINT('Ctrl Pts',(-24.536867432782,20.4806601969072,1.0618816518633));
#42124=CARTESIAN_POINT('Ctrl Pts',(-24.4333070150722,20.4508300704414,1.06844145339731));
#42125=CARTESIAN_POINT('Ctrl Pts',(-24.4243199920023,20.4482836592074,1.06901127139889));
#42126=CARTESIAN_POINT('Ctrl Pts',(-24.4109645552231,20.4445621354021,1.0698589330914));
#42127=CARTESIAN_POINT('Ctrl Pts',(-24.4066044771938,20.4433570763935,1.07013580137979));
#42128=CARTESIAN_POINT('Ctrl Pts',(-24.3991383037835,20.441310450455,1.0706101482528));
#42129=CARTESIAN_POINT('Ctrl Pts',(-24.3960334495205,20.4404643463857,1.07080747900561));
#42130=CARTESIAN_POINT('Ctrl Pts',(-24.3897343058152,20.4387578977413,1.07120797008468));
#42131=CARTESIAN_POINT('Ctrl Pts',(-24.3865399496019,20.4378978185034,1.07141113872544));
#42132=CARTESIAN_POINT('Ctrl Pts',(-24.3792067321786,20.4359354570795,1.07187772517848));
#42133=CARTESIAN_POINT('Ctrl Pts',(-24.375066993221,20.4348365062635,1.07214125081594));
#42134=CARTESIAN_POINT('Ctrl Pts',(-24.3663845020643,20.4325501379371,1.07269423179524));
#42135=CARTESIAN_POINT('Ctrl Pts',(-24.3618413241777,20.4313643899618,1.07298374069533));
#42136=CARTESIAN_POINT('Ctrl Pts',(-24.3498435550139,20.4282610188535,1.07374870835422));
#42137=CARTESIAN_POINT('Ctrl Pts',(-24.3423846902959,20.4263601755973,1.07422471013595));
#42138=CARTESIAN_POINT('Ctrl Pts',(-24.3200325684135,20.4207490834243,1.07565247907355));
#42139=CARTESIAN_POINT('Ctrl Pts',(-24.3051197038885,20.417118529316,1.07660681603012));
#42140=CARTESIAN_POINT('Ctrl Pts',(-24.1371566286211,20.3774964916496,1.08737616900261));
#42141=CARTESIAN_POINT('Ctrl Pts',(-23.9817189932269,20.3526501841446,1.09755131882267));
#42142=CARTESIAN_POINT('Ctrl Pts',(-23.5033041620485,20.3116987966174,1.12944360520425));
#42143=CARTESIAN_POINT('Ctrl Pts',(-23.1792101991778,20.3326829813672,1.15200749182668));
#42144=CARTESIAN_POINT('Ctrl Pts',(-22.8479126284273,20.4049233161702,1.17346161596833));
#42145=CARTESIAN_POINT('Ctrl Pts',(-22.8321944430288,20.4084744012606,1.17447504536514));
#42146=CARTESIAN_POINT('Ctrl Pts',(-22.8127924252049,20.4130109604647,1.17571991996125));
#42147=CARTESIAN_POINT('Ctrl Pts',(-22.8090832014797,20.4138851888562,1.17595763658883));
#42148=CARTESIAN_POINT('Ctrl Pts',(-22.8032471099614,20.4152716309278,1.17633121721482));
#42149=CARTESIAN_POINT('Ctrl Pts',(-22.8011192133105,20.4157794308965,1.17646733569463));
#42150=CARTESIAN_POINT('Ctrl Pts',(-22.7971964829261,20.4167197716297,1.17671809398807));
#42151=CARTESIAN_POINT('Ctrl Pts',(-22.7954015141997,20.4171516855028,1.17683276923952));
#42152=CARTESIAN_POINT('Ctrl Pts',(-22.7914041247192,20.4181171909027,1.17708800166862));
#42153=CARTESIAN_POINT('Ctrl Pts',(-22.7892019004251,20.4186515618189,1.17722851267862));
#42154=CARTESIAN_POINT('Ctrl Pts',(-22.7828438517557,20.4202014486412,1.17763389692923));
#42155=CARTESIAN_POINT('Ctrl Pts',(-22.7786894631304,20.421222922327,1.17789842506234));
#42156=CARTESIAN_POINT('Ctrl Pts',(-22.7506918013589,20.4281660871219,1.17967885723378));
#42157=CARTESIAN_POINT('Ctrl Pts',(-22.726914039097,20.4343521893578,1.18117967427281));
#42158=CARTESIAN_POINT('Ctrl Pts',(-22.6535690912806,20.4543321044506,1.18578075643764));
#42159=CARTESIAN_POINT('Ctrl Pts',(-22.6042575641248,20.4690419501657,1.18883391144853));
#42160=CARTESIAN_POINT('Ctrl Pts',(-22.5136504203636,20.4984510006402,1.19440483147114));
#42161=CARTESIAN_POINT('Ctrl Pts',(-22.472262836203,20.5128235171879,1.19693411092816));
#42162=CARTESIAN_POINT('Ctrl Pts',(-22.1696842245451,20.6248629702744,1.21539685485603));
#42163=CARTESIAN_POINT('Ctrl Pts',(-21.9218615706629,20.7552160898329,1.23047085079505));
#42164=CARTESIAN_POINT('Ctrl Pts',(-21.6017223833773,20.98080430518,1.25313700096463));
#42165=CARTESIAN_POINT('Ctrl Pts',(-21.513024435206,21.0505463005997,1.25980511608295));
#42166=CARTESIAN_POINT('Ctrl Pts',(-21.4202568261997,21.1317103252983,1.26730596167425));
#42167=CARTESIAN_POINT('Ctrl Pts',(-21.4123778127606,21.1386721802291,1.26794737404487));
#42168=CARTESIAN_POINT('Ctrl Pts',(-21.4013426682423,21.1485193564352,1.26885191577603));
#42169=CARTESIAN_POINT('Ctrl Pts',(-21.3981579373047,21.1513726466451,1.26911369722539));
#42170=CARTESIAN_POINT('Ctrl Pts',(-21.3926347690407,21.1563408595619,1.26956897367359));
#42171=CARTESIAN_POINT('Ctrl Pts',(-21.3902937336231,21.1584528966458,1.26976234660244));
#42172=CARTESIAN_POINT('Ctrl Pts',(-21.3854736737971,21.162814309629,1.27016131976304));
#42173=CARTESIAN_POINT('Ctrl Pts',(-21.3829950481802,21.1650641182147,1.27036693820086));
#42174=CARTESIAN_POINT('Ctrl Pts',(-21.3771874950381,21.1703520671661,1.27084978264821));
#42175=CARTESIAN_POINT('Ctrl Pts',(-21.3738614327931,21.1733933312171,1.27112714138503));
#42176=CARTESIAN_POINT('Ctrl Pts',(-21.3668549686429,21.1798268953869,1.27171316240238));
#42177=CARTESIAN_POINT('Ctrl Pts',(-21.3631760713803,21.1832208099192,1.27202189334804));
#42178=CARTESIAN_POINT('Ctrl Pts',(-21.3533125229077,21.1923629134108,1.27285241373305));
#42179=CARTESIAN_POINT('Ctrl Pts',(-21.3471425619303,21.1981268307249,1.27337487805268));
#42180=CARTESIAN_POINT('Ctrl Pts',(-21.1518670228843,21.3819937535564,1.29000503723837));
#42181=CARTESIAN_POINT('Ctrl Pts',(-20.9850061740106,21.5822451677835,1.30716104934124));
#42182=CARTESIAN_POINT('Ctrl Pts',(-20.7304469300662,21.9759106248341,1.33884275640988));
#42183=CARTESIAN_POINT('Ctrl Pts',(-20.6342415915367,22.1621787398352,1.35312090826121));
#42184=CARTESIAN_POINT('Ctrl Pts',(-20.5424689954772,22.392304198516,1.36906515083092));
#42185=CARTESIAN_POINT('Ctrl Pts',(-20.5288211299047,22.4283974795373,1.37151799739849));
#42186=CARTESIAN_POINT('Ctrl Pts',(-20.5142250428256,22.4691987937817,1.37423048981934));
#42187=CARTESIAN_POINT('Ctrl Pts',(-20.5126359373132,22.4736720546063,1.37452706677275));
#42188=CARTESIAN_POINT('Ctrl Pts',(-20.5102569968641,22.4804158667567,1.37497294768239));
#42189=CARTESIAN_POINT('Ctrl Pts',(-20.5094598178541,22.4826837924642,1.37512268640962));
#42190=CARTESIAN_POINT('Ctrl Pts',(-20.5080831815195,22.4866142909213,1.37538182974064));
#42191=CARTESIAN_POINT('Ctrl Pts',(-20.5075025491421,22.4882764462333,1.37549130472152));
#42192=CARTESIAN_POINT('Ctrl Pts',(-20.5062952119632,22.491741765432,1.37571930469514));
#42193=CARTESIAN_POINT('Ctrl Pts',(-20.5056687478071,22.4935450085134,1.37583781474935));
#42194=CARTESIAN_POINT('Ctrl Pts',(-20.5041832586636,22.4978331954764,1.37611932042017));
#42195=CARTESIAN_POINT('Ctrl Pts',(-20.5033256691886,22.5003186432964,1.37628222991182));
#42196=CARTESIAN_POINT('Ctrl Pts',(-20.5004702000861,22.508627266522,1.37682598785116));
#42197=CARTESIAN_POINT('Ctrl Pts',(-20.4984859489215,22.5144551630033,1.37720602762583));
#42198=CARTESIAN_POINT('Ctrl Pts',(-20.443373652309,22.677857320869,1.38782424444582));
#42199=CARTESIAN_POINT('Ctrl Pts',(-20.4024952843724,22.8393294348641,1.39735128594478));
#42200=CARTESIAN_POINT('Ctrl Pts',(-20.3413817849476,23.1941702484797,1.41762717609679));
#42201=CARTESIAN_POINT('Ctrl Pts',(-20.3257824676052,23.3876533650958,1.42829315917424));
#42202=CARTESIAN_POINT('Ctrl Pts',(-20.3290761249458,23.7287952150526,1.44778715597633));
#42203=CARTESIAN_POINT('Ctrl Pts',(-20.3406142673435,23.8759336824188,1.45641622388821));
#42204=CARTESIAN_POINT('Ctrl Pts',(-20.3638118936337,24.0327854257133,1.46606064882687));
#42205=CARTESIAN_POINT('Ctrl Pts',(-20.3655007381437,24.0438089542738,1.46674078353661));
#42206=CARTESIAN_POINT('Ctrl Pts',(-20.3679333606254,24.0591547701043,1.46769090831552));
#42207=CARTESIAN_POINT('Ctrl Pts',(-20.3686288101472,24.0634847296226,1.46795936236115));
#42208=CARTESIAN_POINT('Ctrl Pts',(-20.3698439935893,24.0709532267092,1.46842304296187));
#42209=CARTESIAN_POINT('Ctrl Pts',(-20.3703595420474,24.074092447437,1.46861813621453));
#42210=CARTESIAN_POINT('Ctrl Pts',(-20.3714234686052,24.0805113431904,1.46901745293488));
#42211=CARTESIAN_POINT('Ctrl Pts',(-20.3719722759146,24.0837909418398,1.46922168981802));
#42212=CARTESIAN_POINT('Ctrl Pts',(-20.3732587372041,24.0914062388109,1.4696964330935));
#42213=CARTESIAN_POINT('Ctrl Pts',(-20.3740001913481,24.0957412805185,1.46996706021925));
#42214=CARTESIAN_POINT('Ctrl Pts',(-20.3755787333402,24.1048581602972,1.4705370066209));
#42215=CARTESIAN_POINT('Ctrl Pts',(-20.3764177561066,24.1096396481787,1.4708363870532));
#42216=CARTESIAN_POINT('Ctrl Pts',(-20.3786819471274,24.122373906398,1.47163495301786));
#42217=CARTESIAN_POINT('Ctrl Pts',(-20.3801262169674,24.1303232058794,1.47213474737738));
#42218=CARTESIAN_POINT('Ctrl Pts',(-20.3845912495906,24.1543840712685,1.47365148282445));
#42219=CARTESIAN_POINT('Ctrl Pts',(-20.387705024626,24.1704779097886,1.47467138785947));
#42220=CARTESIAN_POINT('Ctrl Pts',(-20.450877581508,24.4841404582638,1.49465624932366));
#42221=CARTESIAN_POINT('Ctrl Pts',(-20.5525492667497,24.7717109928437,1.51508762909092));
#42222=CARTESIAN_POINT('Ctrl Pts',(-20.7516736320597,25.1534474304713,1.54420754256351));
#42223=CARTESIAN_POINT('Ctrl Pts',(-20.8170882393964,25.2625887684959,1.55276458740409));
#42224=CARTESIAN_POINT('Ctrl Pts',(-20.8919848809947,25.3722741771886,1.56142524484949));
#42225=CARTESIAN_POINT('Ctrl Pts',(-20.8951980175028,25.3769531932459,1.56179480716745));
#42226=CARTESIAN_POINT('Ctrl Pts',(-20.9027130372604,25.3878349563095,1.56265449773609));
#42227=CARTESIAN_POINT('Ctrl Pts',(-20.9070244030506,25.3940311528536,1.56314418028636));
#42228=CARTESIAN_POINT('Ctrl Pts',(-20.9136054742975,25.4034187931727,1.56388626573679));
#42229=CARTESIAN_POINT('Ctrl Pts',(-20.915859264518,25.4066213022014,1.56413945428967));
#42230=CARTESIAN_POINT('Ctrl Pts',(-20.9198030286529,25.4122035228076,1.56458082793997));
#42231=CARTESIAN_POINT('Ctrl Pts',(-20.9214904038212,25.4145850547557,1.56476914512493));
#42232=CARTESIAN_POINT('Ctrl Pts',(-20.9264334852064,25.4215415804054,1.56531926098659));
#42233=CARTESIAN_POINT('Ctrl Pts',(-20.929697933294,25.4261103861867,1.56568060340826));
#42234=CARTESIAN_POINT('Ctrl Pts',(-20.9538565468341,25.4597357864824,1.56834020210734));
#42235=CARTESIAN_POINT('Ctrl Pts',(-20.9752225772096,25.4884525756113,1.57061266592819));
#42236=CARTESIAN_POINT('Ctrl Pts',(-20.9998981955187,25.520489040454,1.57314354692306));
#42237=CARTESIAN_POINT('Ctrl Pts',(-21.0027407281935,25.5241630545311,1.57343372917156));
#42238=CARTESIAN_POINT('Ctrl Pts',(-21.0070503428838,25.5297084780446,1.57387160487157));
#42239=CARTESIAN_POINT('Ctrl Pts',(-21.0085115533534,25.5315844109675,1.57401971166002));
#42240=CARTESIAN_POINT('Ctrl Pts',(-21.0110541964559,25.5348412682416,1.57427680657262));
#42241=CARTESIAN_POINT('Ctrl Pts',(-21.0121346800249,25.5362229267352,1.57438586242916));
#42242=CARTESIAN_POINT('Ctrl Pts',(-21.0143968449302,25.5391107879311,1.57461377889145));
#42243=CARTESIAN_POINT('Ctrl Pts',(-21.0155787396543,25.5406168188192,1.57473262343937));
#42244=CARTESIAN_POINT('Ctrl Pts',(-21.0184054395778,25.5442121439111,1.57501630621624));
#42245=CARTESIAN_POINT('Ctrl Pts',(-21.0200514948338,25.5463004635342,1.5751810547206));
#42246=CARTESIAN_POINT('Ctrl Pts',(-21.0256240980098,25.5533523517118,1.5757373003784));
#42247=CARTESIAN_POINT('Ctrl Pts',(-21.0295627142124,25.5583064310639,1.57612793703275));
#42248=CARTESIAN_POINT('Ctrl Pts',(-21.0389487908096,25.5700413166878,1.5770530135684));
#42249=CARTESIAN_POINT('Ctrl Pts',(-21.0444091909939,25.5768117760394,1.57758654889389));
#42250=CARTESIAN_POINT('Ctrl Pts',(-21.1085514912436,25.655687473222,1.58380111624698));
#42251=CARTESIAN_POINT('Ctrl Pts',(-21.1703058013761,25.7252507930029,1.58927146175341));
#42252=CARTESIAN_POINT('Ctrl Pts',(-21.3528530117786,25.9137801020719,1.60438821959014));
#42253=CARTESIAN_POINT('Ctrl Pts',(-21.4801406929185,26.026029351804,1.61375622192197));
#42254=CARTESIAN_POINT('Ctrl Pts',(-21.6965110233861,26.1884292900875,1.628905197601));
#42255=CARTESIAN_POINT('Ctrl Pts',(-21.7801575944174,26.245265818469,1.6345967792353));
#42256=CARTESIAN_POINT('Ctrl Pts',(-21.9344422770162,26.3398144572332,1.64498041584185));
#42257=CARTESIAN_POINT('Ctrl Pts',(-22.0040585157554,26.3789933939254,1.64962651365814));
#42258=CARTESIAN_POINT('Ctrl Pts',(-22.0750360931093,26.4155368145933,1.65435918102699));
#42259=CARTESIAN_POINT('Origin',(-23.5502525316942,23.5502525316942,-77.3107734492734));
#42260=CARTESIAN_POINT('',(-22.0750360153455,26.415536774556,3.15065971150053));
#42261=CARTESIAN_POINT('',(-22.0750360171757,26.4155367754983,2.90599376073416));
#42262=CARTESIAN_POINT('',(-22.0750360153461,26.4155367745563,-77.3107734492734));
#42263=CARTESIAN_POINT('Ctrl Pts',(-22.0750360153455,26.415536774556,3.15065971150053));
#42264=CARTESIAN_POINT('Ctrl Pts',(-22.0689721537274,26.4124147426549,3.15022964192226));
#42265=CARTESIAN_POINT('Ctrl Pts',(-22.0629181479893,26.4092734328418,3.14980069220542));
#42266=CARTESIAN_POINT('Ctrl Pts',(-22.0526714943233,26.4039152816198,3.14907545024222));
#42267=CARTESIAN_POINT('Ctrl Pts',(-22.0484737222784,26.4017083812685,3.14877855940214));
#42268=CARTESIAN_POINT('Ctrl Pts',(-22.040876312398,26.3976927540212,3.14824164812645));
#42269=CARTESIAN_POINT('Ctrl Pts',(-22.0374750258636,26.3958871901358,3.14800143178819));
#42270=CARTESIAN_POINT('Ctrl Pts',(-22.0321711014334,26.3930594189751,3.14762709115791));
#42271=CARTESIAN_POINT('Ctrl Pts',(-22.0302662554384,26.3920413956555,3.14749270123395));
#42272=CARTESIAN_POINT('Ctrl Pts',(-22.0268765330157,26.3902254137327,3.1472536426412));
#42273=CARTESIAN_POINT('Ctrl Pts',(-22.0253912658919,26.3894282085682,3.14714892641721));
#42274=CARTESIAN_POINT('Ctrl Pts',(-22.0219857030607,26.3875968569275,3.14690889530204));
#42275=CARTESIAN_POINT('Ctrl Pts',(-22.0200658348211,26.3865619281134,3.14677363152521));
#42276=CARTESIAN_POINT('Ctrl Pts',(-22.0148191415902,26.383726755263,3.14640411680164));
#42277=CARTESIAN_POINT('Ctrl Pts',(-22.0114944197689,26.3819225944676,3.14617011652517));
#42278=CARTESIAN_POINT('Ctrl Pts',(-21.9954016433121,26.3731531348337,3.14503818338911));
#42279=CARTESIAN_POINT('Ctrl Pts',(-21.9826773988296,26.3661071660755,3.14414534600292));
#42280=CARTESIAN_POINT('Ctrl Pts',(-21.7433708370467,26.2314678259684,3.12738619663064));
#42281=CARTESIAN_POINT('Ctrl Pts',(-21.5329637759489,26.0769760630842,3.11315439362061));
#42282=CARTESIAN_POINT('Ctrl Pts',(-21.3141500402638,25.8713672050449,3.09634236253687));
#42283=CARTESIAN_POINT('Ctrl Pts',(-21.285423912797,25.8433462801086,3.09409070725609));
#42284=CARTESIAN_POINT('Ctrl Pts',(-21.2293461717112,25.786563286217,3.08959199488535));
#42285=CARTESIAN_POINT('Ctrl Pts',(-21.2019878466722,25.7578179296223,3.08734556221746));
#42286=CARTESIAN_POINT('Ctrl Pts',(-21.1090899986132,25.6565288653715,3.07951567208062));
#42287=CARTESIAN_POINT('Ctrl Pts',(-21.0463294478684,25.5815184751539,3.07386308807352));
#42288=CARTESIAN_POINT('Ctrl Pts',(-20.9485797025379,25.4532632360276,3.06432045148484));
#42289=CARTESIAN_POINT('Ctrl Pts',(-20.9115851026535,25.401626236491,3.06050921505357));
#42290=CARTESIAN_POINT('Ctrl Pts',(-20.8714560090935,25.3419660256991,3.05612641706771));
#42291=CARTESIAN_POINT('Ctrl Pts',(-20.8667973544679,25.3349811844064,3.05561361119816));
#42292=CARTESIAN_POINT('Ctrl Pts',(-20.8598383058753,25.3244584565067,3.05484151159028));
#42293=CARTESIAN_POINT('Ctrl Pts',(-20.857517454265,25.3209340876618,3.05458298789678));
#42294=CARTESIAN_POINT('Ctrl Pts',(-20.8535369766745,25.3148635412927,3.05413781855784));
#42295=CARTESIAN_POINT('Ctrl Pts',(-20.8518740140117,25.3123195494567,3.05395129838414));
#42296=CARTESIAN_POINT('Ctrl Pts',(-20.848455866772,25.3070742988103,3.0535668029335));
#42297=CARTESIAN_POINT('Ctrl Pts',(-20.8467011290866,25.3043727537227,3.05336881118368));
#42298=CARTESIAN_POINT('Ctrl Pts',(-20.8424851889798,25.2978606565605,3.05289164673333));
#42299=CARTESIAN_POINT('Ctrl Pts',(-20.8400279805272,25.2940475375058,3.052612325216));
#42300=CARTESIAN_POINT('Ctrl Pts',(-20.8325073753402,25.2823226980185,3.051753682763));
#42301=CARTESIAN_POINT('Ctrl Pts',(-20.8274705454366,25.2743940712053,3.05117337427904));
#42302=CARTESIAN_POINT('Ctrl Pts',(-20.8090347183839,25.2450914162827,3.04902978475394));
#42303=CARTESIAN_POINT('Ctrl Pts',(-20.7958524334708,25.2235827397628,3.04745852246808));
#42304=CARTESIAN_POINT('Ctrl Pts',(-20.7798318805004,25.19674072985,3.0454998808657));
#42305=CARTESIAN_POINT('Ctrl Pts',(-20.7767540293872,25.1915508068804,3.04512127903175));
#42306=CARTESIAN_POINT('Ctrl Pts',(-20.7702056904868,25.1804378737726,3.04431080894755));
#42307=CARTESIAN_POINT('Ctrl Pts',(-20.7667395209942,25.1745123652567,3.04387878760487));
#42308=CARTESIAN_POINT('Ctrl Pts',(-20.7625236947278,25.1672521720804,3.04334960651454));
#42309=CARTESIAN_POINT('Ctrl Pts',(-20.7617560017088,25.165927934648,3.0432530915796));
#42310=CARTESIAN_POINT('Ctrl Pts',(-20.7595646366385,25.1621417099947,3.04297715593653));
#42311=CARTESIAN_POINT('Ctrl Pts',(-20.7581432823337,25.1596783890376,3.0427976528693));
#42312=CARTESIAN_POINT('Ctrl Pts',(-20.7532891039878,25.1512399249171,3.04218280947059));
#42313=CARTESIAN_POINT('Ctrl Pts',(-20.7498722027233,25.1452556856467,3.04174690651847));
#42314=CARTESIAN_POINT('Ctrl Pts',(-20.7438546457933,25.1346378075357,3.04097368767491));
#42315=CARTESIAN_POINT('Ctrl Pts',(-20.741246198937,25.1300085945988,3.04063664683799));
#42316=CARTESIAN_POINT('Ctrl Pts',(-20.7366916515578,25.1218786890185,3.04004484873125));
#42317=CARTESIAN_POINT('Ctrl Pts',(-20.7347406011122,25.1183807704364,3.03979026414752));
#42318=CARTESIAN_POINT('Ctrl Pts',(-20.7306790806224,25.1110671044611,3.03925804211906));
#42319=CARTESIAN_POINT('Ctrl Pts',(-20.7285698251872,25.1072506948443,3.03898036350651));
#42320=CARTESIAN_POINT('Ctrl Pts',(-20.7165802888827,25.0854528879501,3.03739462723167));
#42321=CARTESIAN_POINT('Ctrl Pts',(-20.7068643288012,25.0673820617276,3.0360809957412));
#42322=CARTESIAN_POINT('Ctrl Pts',(-20.5571028786504,24.7823464917123,3.01537566723813));
#42323=CARTESIAN_POINT('Ctrl Pts',(-20.4550399136743,24.4971407629173,2.99465608499176));
#42324=CARTESIAN_POINT('Ctrl Pts',(-20.3764571954094,24.1165968855771,2.9686593208174));
#42325=CARTESIAN_POINT('Ctrl Pts',(-20.3622932004324,24.0305030390971,2.96289687013642));
#42326=CARTESIAN_POINT('Ctrl Pts',(-20.3484551062746,23.9180702671479,2.955608582127));
#42327=CARTESIAN_POINT('Ctrl Pts',(-20.3455855043574,23.8921677006739,2.95394576427495));
#42328=CARTESIAN_POINT('Ctrl Pts',(-20.3420781918439,23.8565681674941,2.95168534573581));
#42329=CARTESIAN_POINT('Ctrl Pts',(-20.3411697441133,23.8468996818152,2.95107395396739));
#42330=CARTESIAN_POINT('Ctrl Pts',(-20.3398872601461,23.8325544861959,2.9501707050421));
#42331=CARTESIAN_POINT('Ctrl Pts',(-20.3394797213011,23.8278809361704,2.9498770435787));
#42332=CARTESIAN_POINT('Ctrl Pts',(-20.3388470368081,23.8204377114764,2.94941033903733));
#42333=CARTESIAN_POINT('Ctrl Pts',(-20.3386152677574,23.8176686288011,2.94923693003962));
#42334=CARTESIAN_POINT('Ctrl Pts',(-20.3381868835839,23.8124695755081,2.94891176165231));
#42335=CARTESIAN_POINT('Ctrl Pts',(-20.3379894439835,23.8100396777581,2.94875995612464));
#42336=CARTESIAN_POINT('Ctrl Pts',(-20.3376456538787,23.8057483193702,2.94849215962291));
#42337=CARTESIAN_POINT('Ctrl Pts',(-20.3374981636527,23.8038869528748,2.94837610386146));
#42338=CARTESIAN_POINT('Ctrl Pts',(-20.337214412085,23.8002659697631,2.94815053279951));
#42339=CARTESIAN_POINT('Ctrl Pts',(-20.33707797875,23.7985063728052,2.94804100780829));
#42340=CARTESIAN_POINT('Ctrl Pts',(-20.336757855954,23.7943332363309,2.94778146521344));
#42341=CARTESIAN_POINT('Ctrl Pts',(-20.3365754397179,23.7919195960264,2.94763151995224));
#42342=CARTESIAN_POINT('Ctrl Pts',(-20.3359446471403,23.7834462426487,2.94710570236284));
#42343=CARTESIAN_POINT('Ctrl Pts',(-20.3355106857597,23.7773854200154,2.94673064004958));
#42344=CARTESIAN_POINT('Ctrl Pts',(-20.3302010473401,23.7001643273391,2.94196485483842));
#42345=CARTESIAN_POINT('Ctrl Pts',(-20.3276715073951,23.6288559289507,2.93770334010832));
#42346=CARTESIAN_POINT('Ctrl Pts',(-20.3269424239474,23.3053742697196,2.91876680886396));
#42347=CARTESIAN_POINT('Ctrl Pts',(-20.3559658256038,23.0540158032507,2.90508084240943));
#42348=CARTESIAN_POINT('Ctrl Pts',(-20.4557113981276,22.6322227833925,2.88057621796159));
#42349=CARTESIAN_POINT('Ctrl Pts',(-20.5122153191156,22.4597119715439,2.87009053832727));
#42350=CARTESIAN_POINT('Ctrl Pts',(-20.5881425499942,22.2805273881455,2.85826920850269));
#42351=CARTESIAN_POINT('Ctrl Pts',(-20.5934528877796,22.2682098876806,2.85745182678728));
#42352=CARTESIAN_POINT('Ctrl Pts',(-20.6008907775414,22.2512494979094,2.85631963439452));
#42353=CARTESIAN_POINT('Ctrl Pts',(-20.6029527538395,22.2465778569291,2.85600707222182));
#42354=CARTESIAN_POINT('Ctrl Pts',(-20.6064489628958,22.2387074887493,2.85547929505755));
#42355=CARTESIAN_POINT('Ctrl Pts',(-20.6078773322964,22.2355061541909,2.85526428183323));
#42356=CARTESIAN_POINT('Ctrl Pts',(-20.6107114011699,22.2291820444765,2.85483886488087));
#42357=CARTESIAN_POINT('Ctrl Pts',(-20.6121168606885,22.2260591663374,2.85462846963384));
#42358=CARTESIAN_POINT('Ctrl Pts',(-20.6152221630272,22.2191885842099,2.85416487070892));
#42359=CARTESIAN_POINT('Ctrl Pts',(-20.6169242101374,22.2154418878204,2.8539115912183));
#42360=CARTESIAN_POINT('Ctrl Pts',(-20.6228760376224,22.2024065598085,2.85302875609248));
#42361=CARTESIAN_POINT('Ctrl Pts',(-20.6271627655735,22.1931349548728,2.85239792463933));
#42362=CARTESIAN_POINT('Ctrl Pts',(-20.6423101124016,22.1607780511513,2.85018612422393));
#42363=CARTESIAN_POINT('Ctrl Pts',(-20.6534004946194,22.1378019446303,2.84859719965345));
#42364=CARTESIAN_POINT('Ctrl Pts',(-20.6674548415714,22.1095472902474,2.84661994454605));
#42365=CARTESIAN_POINT('Ctrl Pts',(-20.6701626528781,22.104141746157,2.84624060257306));
#42366=CARTESIAN_POINT('Ctrl Pts',(-20.6759740957533,22.0926215576172,2.84542987653227));
#42367=CARTESIAN_POINT('Ctrl Pts',(-20.6790820603179,22.0865091433128,2.84499834296387));
#42368=CARTESIAN_POINT('Ctrl Pts',(-20.6827674864684,22.0793179394242,2.84448901733501));
#42369=CARTESIAN_POINT('Ctrl Pts',(-20.6833261023039,22.0782294653711,2.84441188075273));
#42370=CARTESIAN_POINT('Ctrl Pts',(-20.6853245553638,22.0743408925264,2.84413615262193));
#42371=CARTESIAN_POINT('Ctrl Pts',(-20.6867678726063,22.0715425928465,2.84393744035542));
#42372=CARTESIAN_POINT('Ctrl Pts',(-20.6913805207197,22.0626316807603,2.84330372661108));
#42373=CARTESIAN_POINT('Ctrl Pts',(-20.6945653254068,22.0565271386129,2.84286818975382));
#42374=CARTESIAN_POINT('Ctrl Pts',(-20.7002716026716,22.0456744615713,2.84209138237212));
#42375=CARTESIAN_POINT('Ctrl Pts',(-20.7027854471277,22.0409223270538,2.84175037633165));
#42376=CARTESIAN_POINT('Ctrl Pts',(-20.7071924493217,22.0326415915818,2.84115465782254));
#42377=CARTESIAN_POINT('Ctrl Pts',(-20.7090803201243,22.0291101775728,2.8409001275841));
#42378=CARTESIAN_POINT('Ctrl Pts',(-20.7130649832219,22.0216898415878,2.84036428920416));
#42379=CARTESIAN_POINT('Ctrl Pts',(-20.7151631993905,22.0178016971348,2.84008293270806));
#42380=CARTESIAN_POINT('Ctrl Pts',(-20.7260501142702,21.9977263531866,2.83862719602005));
#42381=CARTESIAN_POINT('Ctrl Pts',(-20.7349693362382,21.9816106551079,2.83744838088159));
#42382=CARTESIAN_POINT('Ctrl Pts',(-20.772053045677,21.9159410636299,2.83260278937207));
#42383=CARTESIAN_POINT('Ctrl Pts',(-20.8013903677834,21.8670643195113,2.82889720740297));
#42384=CARTESIAN_POINT('Ctrl Pts',(-20.9688285275158,21.6041700932044,2.80842519191634));
#42385=CARTESIAN_POINT('Ctrl Pts',(-21.1306312700497,21.4063318484599,2.79091448301039));
#42386=CARTESIAN_POINT('Ctrl Pts',(-21.3454192871674,21.1993522303183,2.77100760994721));
#42387=CARTESIAN_POINT('Ctrl Pts',(-21.3774550961832,21.1697119523398,2.76811511240939));
#42388=CARTESIAN_POINT('Ctrl Pts',(-21.4593947981516,21.0969320596152,2.76092537542677));
#42389=CARTESIAN_POINT('Ctrl Pts',(-21.5100426272231,21.0546539250662,2.75666744327902));
#42390=CARTESIAN_POINT('Ctrl Pts',(-21.5675703144586,21.0095558413595,2.75206513374346));
#42391=CARTESIAN_POINT('Ctrl Pts',(-21.5731988809698,21.0051734933854,2.7516172509516));
#42392=CARTESIAN_POINT('Ctrl Pts',(-21.581804403983,20.9985190906363,2.75093621106533));
#42393=CARTESIAN_POINT('Ctrl Pts',(-21.5847708022651,20.9962335111466,2.75070212281107));
#42394=CARTESIAN_POINT('Ctrl Pts',(-21.5896329553253,20.9925007596707,2.75031954237935));
#42395=CARTESIAN_POINT('Ctrl Pts',(-21.5915263342834,20.9910505204816,2.75017083531332));
#42396=CARTESIAN_POINT('Ctrl Pts',(-21.5951799212701,20.9882584744809,2.74988441159942));
#42397=CARTESIAN_POINT('Ctrl Pts',(-21.5969399042142,20.9869163772609,2.74974667440132));
#42398=CARTESIAN_POINT('Ctrl Pts',(-21.6001554895538,20.9844695268482,2.7494954555577));
#42399=CARTESIAN_POINT('Ctrl Pts',(-21.6016106433871,20.9833642028217,2.74938193340587));
#42400=CARTESIAN_POINT('Ctrl Pts',(-21.6045788672066,20.9811135407211,2.74915070150007));
#42401=CARTESIAN_POINT('Ctrl Pts',(-21.6060920029518,20.9799683057487,2.74903299910886));
#42402=CARTESIAN_POINT('Ctrl Pts',(-21.610444454988,20.9766801426103,2.74869493333451));
#42403=CARTESIAN_POINT('Ctrl Pts',(-21.6132863203137,20.9745405694263,2.74847480779296));
#42404=CARTESIAN_POINT('Ctrl Pts',(-21.6257274864736,20.9652061443529,2.74751377052465));
#42405=CARTESIAN_POINT('Ctrl Pts',(-21.6353635367135,20.9580600963296,2.74677625640235));
#42406=CARTESIAN_POINT('Ctrl Pts',(-21.7999902990395,20.8373926414277,2.73428785024807));
#42407=CARTESIAN_POINT('Ctrl Pts',(-21.9648133467986,20.737881099687,2.72344874089343));
#42408=CARTESIAN_POINT('Ctrl Pts',(-22.2785489645164,20.5848690740442,2.70390723880978));
#42409=CARTESIAN_POINT('Ctrl Pts',(-22.4243848025181,20.5264884993281,2.69520320136931));
#42410=CARTESIAN_POINT('Ctrl Pts',(-22.7048443569871,20.4373301474084,2.6784045860549));
#42411=CARTESIAN_POINT('Ctrl Pts',(-22.8383155569215,20.4041216671813,2.67038723780692));
#42412=CARTESIAN_POINT('Ctrl Pts',(-22.9947874137189,20.3756588959988,2.66077397949195));
#42413=CARTESIAN_POINT('Ctrl Pts',(-23.0161251445854,20.371999214558,2.65945871810378));
#42414=CARTESIAN_POINT('Ctrl Pts',(-23.0435465004669,20.3675800543144,2.65776242504027));
#42415=CARTESIAN_POINT('Ctrl Pts',(-23.0495980038037,20.3666225055705,2.65738770149755));
#42416=CARTESIAN_POINT('Ctrl Pts',(-23.0593372100511,20.365109894924,2.65678400972904));
#42417=CARTESIAN_POINT('Ctrl Pts',(-23.0630232303135,20.3645439641561,2.65655538709327));
#42418=CARTESIAN_POINT('Ctrl Pts',(-23.070034684972,20.3634799183996,2.65612023372526));
#42419=CARTESIAN_POINT('Ctrl Pts',(-23.07335993512,20.3629806072498,2.65591374127966));
#42420=CARTESIAN_POINT('Ctrl Pts',(-23.0809274023555,20.3618564031667,2.65544354598459));
#42421=CARTESIAN_POINT('Ctrl Pts',(-23.0851700909536,20.3612347718708,2.65517974000688));
#42422=CARTESIAN_POINT('Ctrl Pts',(-23.0980564192259,20.3593729524745,2.65437789225759));
#42423=CARTESIAN_POINT('Ctrl Pts',(-23.1067038173636,20.3581594332991,2.65383900598652));
#42424=CARTESIAN_POINT('Ctrl Pts',(-23.1678064614015,20.3498377700616,2.6500254162419));
#42425=CARTESIAN_POINT('Ctrl Pts',(-23.2204222695272,20.3439881784692,2.64671108664128));
#42426=CARTESIAN_POINT('Ctrl Pts',(-23.2769420682005,20.3391104614585,2.64311542582022));
#42427=CARTESIAN_POINT('Ctrl Pts',(-23.2807288452817,20.338790405659,2.642874350809));
#42428=CARTESIAN_POINT('Ctrl Pts',(-23.2885442600985,20.3381437726874,2.64237645388914));
#42429=CARTESIAN_POINT('Ctrl Pts',(-23.2925729622165,20.3378180750325,2.64211960566326));
#42430=CARTESIAN_POINT('Ctrl Pts',(-23.3020705349442,20.3370682314249,2.64151363919007));
#42431=CARTESIAN_POINT('Ctrl Pts',(-23.3075398844313,20.3366504683894,2.64116432873499));
#42432=CARTESIAN_POINT('Ctrl Pts',(-23.3338180169029,20.3347107444266,2.63948432190373));
#42433=CARTESIAN_POINT('Ctrl Pts',(-23.3546398202615,20.3333769481231,2.63814801259008));
#42434=CARTESIAN_POINT('Ctrl Pts',(-23.6327443200828,20.3182722428812,2.62023095267543));
#42435=CARTESIAN_POINT('Ctrl Pts',(-23.8907314595865,20.3352043635715,2.60271318911965));
#42436=CARTESIAN_POINT('Ctrl Pts',(-24.3019792165563,20.412276625361,2.5744736292064));
#42437=CARTESIAN_POINT('Ctrl Pts',(-24.4576458760638,20.4537001016352,2.5637382030774));
#42438=CARTESIAN_POINT('Ctrl Pts',(-24.6162766012742,20.5089106498502,2.55316376842186));
#42439=CARTESIAN_POINT('Ctrl Pts',(-24.6229602475664,20.5112615942764,2.55271894661977));
#42440=CARTESIAN_POINT('Ctrl Pts',(-24.6331472774998,20.5148826337123,2.55204211241467));
#42441=CARTESIAN_POINT('Ctrl Pts',(-24.6366562486586,20.5161367771185,2.55180918252031));
#42442=CARTESIAN_POINT('Ctrl Pts',(-24.6424002090563,20.5182009713589,2.55142824286814));
#42443=CARTESIAN_POINT('Ctrl Pts',(-24.6446364789671,20.5190074096796,2.55128002079108));
#42444=CARTESIAN_POINT('Ctrl Pts',(-24.6489477360105,20.520567517695,2.55099443812415));
#42445=CARTESIAN_POINT('Ctrl Pts',(-24.6510228439927,20.5213208461536,2.55085705728554));
#42446=CARTESIAN_POINT('Ctrl Pts',(-24.6548418817534,20.5227117181044,2.55060436447167));
#42447=CARTESIAN_POINT('Ctrl Pts',(-24.6565860273068,20.5233486338562,2.5504890155984));
#42448=CARTESIAN_POINT('Ctrl Pts',(-24.6601233928109,20.5246438519276,2.55025518457493));
#42449=CARTESIAN_POINT('Ctrl Pts',(-24.6619165708145,20.5253022386135,2.55013670819908));
#42450=CARTESIAN_POINT('Ctrl Pts',(-24.667105904519,20.5272128019058,2.54979401178729));
#42451=CARTESIAN_POINT('Ctrl Pts',(-24.6705005513344,20.5284691114162,2.54957004005036));
#42452=CARTESIAN_POINT('Ctrl Pts',(-24.6856534748635,20.5341060321116,2.54857117202522));
#42453=CARTESIAN_POINT('Ctrl Pts',(-24.6973884324667,20.53854965026,2.54780001037813));
#42454=CARTESIAN_POINT('Ctrl Pts',(-24.9003443661025,20.6167603306567,2.53449948607699));
#42455=CARTESIAN_POINT('Ctrl Pts',(-25.0841584152696,20.7085479419708,2.52300387903064));
#42456=CARTESIAN_POINT('Ctrl Pts',(-25.3229680226129,20.8577702272276,2.50725855860012));
#42457=CARTESIAN_POINT('Ctrl Pts',(-25.3864398157547,20.9006492952285,2.50298891462022));
#42458=CARTESIAN_POINT('Ctrl Pts',(-25.5144690768732,20.9939525042213,2.49409473620066));
#42459=CARTESIAN_POINT('Ctrl Pts',(-25.5787518894796,21.044657606144,2.48946914396926));
#42460=CARTESIAN_POINT('Ctrl Pts',(-25.7448850891645,21.1862878022225,2.47694431740816));
#42461=CARTESIAN_POINT('Ctrl Pts',(-25.8429963801582,21.2813189440096,2.468928168689));
#42462=CARTESIAN_POINT('Ctrl Pts',(-25.9419952961084,21.3902064499884,2.45997273913193));
#42463=CARTESIAN_POINT('Ctrl Pts',(-25.9491684741101,21.398175668969,2.45931860369201));
#42464=CARTESIAN_POINT('Ctrl Pts',(-25.9594046206718,21.4096625364474,2.45837751119456));
#42465=CARTESIAN_POINT('Ctrl Pts',(-25.9624999830549,21.4131513294537,2.45809191633621));
#42466=CARTESIAN_POINT('Ctrl Pts',(-25.9678515834599,21.4192095757467,2.45759638307381));
#42467=CARTESIAN_POINT('Ctrl Pts',(-25.9701113314562,21.4217759299293,2.45738659197696));
#42468=CARTESIAN_POINT('Ctrl Pts',(-25.9744434021122,21.4267115986118,2.45698335137484));
#42469=CARTESIAN_POINT('Ctrl Pts',(-25.9765163475088,21.4290803636121,2.4567899281768));
#42470=CARTESIAN_POINT('Ctrl Pts',(-25.9813837750523,21.4346588675747,2.45633465160916));
#42471=CARTESIAN_POINT('Ctrl Pts',(-25.9841753716075,21.4378711070522,2.45607267859472));
#42472=CARTESIAN_POINT('Ctrl Pts',(-25.9937667756515,21.4489520163954,2.45516961196423));
#42473=CARTESIAN_POINT('Ctrl Pts',(-26.0005347983614,21.4568480018427,2.45452720404576));
#42474=CARTESIAN_POINT('Ctrl Pts',(-26.0770143390037,21.546952678605,2.44720843883806));
#42475=CARTESIAN_POINT('Ctrl Pts',(-26.142590106918,21.6325672188292,2.44036418546625));
#42476=CARTESIAN_POINT('Ctrl Pts',(-26.3646992842135,21.9548091315217,2.41494661787555));
#42477=CARTESIAN_POINT('Ctrl Pts',(-26.494109373313,22.2085321106504,2.39543037561156));
#42478=CARTESIAN_POINT('Ctrl Pts',(-26.6102744240062,22.5370411598884,2.37216360277266));
#42479=CARTESIAN_POINT('Ctrl Pts',(-26.6300627015075,22.5988842638521,2.3678722440661));
#42480=CARTESIAN_POINT('Ctrl Pts',(-26.6586447740323,22.6984821949141,2.36114326187468));
#42481=CARTESIAN_POINT('Ctrl Pts',(-26.6686488016687,22.7358692992355,2.35865760711562));
#42482=CARTESIAN_POINT('Ctrl Pts',(-26.6821667513215,22.7902966523856,2.35510594295059));
#42483=CARTESIAN_POINT('Ctrl Pts',(-26.686219624897,22.8071979978633,2.35401231520406));
#42484=CARTESIAN_POINT('Ctrl Pts',(-26.6910058652513,22.8278946034136,2.35268511644715));
#42485=CARTESIAN_POINT('Ctrl Pts',(-26.6918692932622,22.8316590425732,2.3524442007248));
#42486=CARTESIAN_POINT('Ctrl Pts',(-26.6932085887111,22.8375467573781,2.35206816665482));
#42487=CARTESIAN_POINT('Ctrl Pts',(-26.6936890728281,22.8396689623556,2.35193278213363));
#42488=CARTESIAN_POINT('Ctrl Pts',(-26.6945360554288,22.8434275908204,2.35169328056941));
#42489=CARTESIAN_POINT('Ctrl Pts',(-26.6949034239572,22.8450638048369,2.35158911343179));
#42490=CARTESIAN_POINT('Ctrl Pts',(-26.695687185334,22.848567372579,2.35136626319743));
#42491=CARTESIAN_POINT('Ctrl Pts',(-26.6961031913151,22.8504348052461,2.35124760295276));
#42492=CARTESIAN_POINT('Ctrl Pts',(-26.6973046546765,22.8558508415949,2.35090380523861));
#42493=CARTESIAN_POINT('Ctrl Pts',(-26.6980857756069,22.8594004195836,2.3506789185853));
#42494=CARTESIAN_POINT('Ctrl Pts',(-26.7015655249497,22.8753415642943,2.34967086322423));
#42495=CARTESIAN_POINT('Ctrl Pts',(-26.7041970484542,22.8877478953697,2.348891513586));
#42496=CARTESIAN_POINT('Ctrl Pts',(-26.7505982872837,23.1130509302846,2.33482674281852));
#42497=CARTESIAN_POINT('Ctrl Pts',(-26.7728007868959,23.3298597703338,2.32270222717392));
#42498=CARTESIAN_POINT('Ctrl Pts',(-26.7732534614922,23.8210445038373,2.29525433934036));
#42499=CARTESIAN_POINT('Ctrl Pts',(-26.7386261652086,24.0936773121162,2.27994883779347));
#42500=CARTESIAN_POINT('Ctrl Pts',(-26.6656921857838,24.3751427893889,2.26233004103553));
#42501=CARTESIAN_POINT('Ctrl Pts',(-26.6612852519656,24.3916107024465,2.26129289263315));
#42502=CARTESIAN_POINT('Ctrl Pts',(-26.6551987142132,24.4136531595913,2.25989592550752));
#42503=CARTESIAN_POINT('Ctrl Pts',(-26.6536343028905,24.4192594488681,2.25953985970554));
#42504=CARTESIAN_POINT('Ctrl Pts',(-26.6511605977192,24.4280324490498,2.25898146788909));
#42505=CARTESIAN_POINT('Ctrl Pts',(-26.6502616153487,24.4312020753012,2.25877947848115));
#42506=CARTESIAN_POINT('Ctrl Pts',(-26.6485295020142,24.4372736662859,2.25839208260559));
#42507=CARTESIAN_POINT('Ctrl Pts',(-26.6476971499433,24.4401758513172,2.25820670174519));
#42508=CARTESIAN_POINT('Ctrl Pts',(-26.6457367888559,24.4469750278694,2.25777190598687));
#42509=CARTESIAN_POINT('Ctrl Pts',(-26.6446054989195,24.4508710610771,2.25752238405177));
#42510=CARTESIAN_POINT('Ctrl Pts',(-26.6413292021852,24.4620752059601,2.25680372128216));
#42511=CARTESIAN_POINT('Ctrl Pts',(-26.6391656517284,24.4693778264411,2.25633397405694));
#42512=CARTESIAN_POINT('Ctrl Pts',(-26.6246364512801,24.5177874262614,2.25321101179727));
#42513=CARTESIAN_POINT('Ctrl Pts',(-26.6114769339192,24.5586498387803,2.25053183787184));
#42514=CARTESIAN_POINT('Ctrl Pts',(-26.57079659377,24.6768245622434,2.242652689255));
#42515=CARTESIAN_POINT('Ctrl Pts',(-26.5411360292892,24.7533589089354,2.23738351289304));
#42516=CARTESIAN_POINT('Ctrl Pts',(-26.3901212993046,25.1028155001723,2.2125409862792));
#42517=CARTESIAN_POINT('Ctrl Pts',(-26.2341490767717,25.3591093719883,2.19187166848193));
#42518=CARTESIAN_POINT('Ctrl Pts',(-25.9886019742628,25.6594112886723,2.16622098097852));
#42519=CARTESIAN_POINT('Ctrl Pts',(-25.9291939559346,25.7261982629153,2.16042209515106));
#42520=CARTESIAN_POINT('Ctrl Pts',(-25.8626303357909,25.7950392583061,2.15441903218325));
#42521=CARTESIAN_POINT('Ctrl Pts',(-25.8581659784763,25.7996289076443,2.15401868144554));
#42522=CARTESIAN_POINT('Ctrl Pts',(-25.8519562591376,25.8059749534546,2.15346498815783));
#42523=CARTESIAN_POINT('Ctrl Pts',(-25.8502225448128,25.8077426494613,2.15331074199663));
#42524=CARTESIAN_POINT('Ctrl Pts',(-25.8472393155269,25.8107773477347,2.15304591733451));
#42525=CARTESIAN_POINT('Ctrl Pts',(-25.8459907886789,25.8120453127617,2.15293526102146));
#42526=CARTESIAN_POINT('Ctrl Pts',(-25.8434097779198,25.814662168129,2.15270687355758));
#42527=CARTESIAN_POINT('Ctrl Pts',(-25.8420771563221,25.8160109141038,2.15258915440102));
#42528=CARTESIAN_POINT('Ctrl Pts',(-25.8389459727108,25.8191743954021,2.15231302680414));
#42529=CARTESIAN_POINT('Ctrl Pts',(-25.8371464367368,25.8209881741131,2.15215469568438));
#42530=CARTESIAN_POINT('Ctrl Pts',(-25.8312965912847,25.8268703118931,2.15164117102741));
#42531=CARTESIAN_POINT('Ctrl Pts',(-25.8272375383268,25.830930018689,2.15128666772739));
#42532=CARTESIAN_POINT('Ctrl Pts',(-25.7129072489442,25.944669258645,2.14135163191842));
#42533=CARTESIAN_POINT('Ctrl Pts',(-25.5948330493108,26.0462517874045,2.1323948248655));
#42534=CARTESIAN_POINT('Ctrl Pts',(-25.1958131932324,26.3421429410736,2.10434042053071));
#42535=CARTESIAN_POINT('Ctrl Pts',(-24.8912647174764,26.5005408384653,2.08581638661141));
#42536=CARTESIAN_POINT('Ctrl Pts',(-24.5484308419812,26.6145898302528,2.0639632193382));
#42537=CARTESIAN_POINT('Ctrl Pts',(-24.5292655875258,26.6207665646138,2.06273954923233));
#42538=CARTESIAN_POINT('Ctrl Pts',(-24.5042221416756,26.6285794700039,2.06113752925753));
#42539=CARTESIAN_POINT('Ctrl Pts',(-24.4983951302862,26.6303792121765,2.06076456463829));
#42540=CARTESIAN_POINT('Ctrl Pts',(-24.4889468617728,26.6332680711803,2.06015946016757));
#42541=CARTESIAN_POINT('Ctrl Pts',(-24.4853287156753,26.6343673791005,2.05992765512354));
#42542=CARTESIAN_POINT('Ctrl Pts',(-24.4785627257672,26.6364101013998,2.05949401460952));
#42543=CARTESIAN_POINT('Ctrl Pts',(-24.4754153546328,26.6373550749208,2.05929223056917));
#42544=CARTESIAN_POINT('Ctrl Pts',(-24.4683586880135,26.6394620229787,2.05883966549198));
#42545=CARTESIAN_POINT('Ctrl Pts',(-24.464448626224,26.6406213924964,2.05858879951207));
#42546=CARTESIAN_POINT('Ctrl Pts',(-24.4562988952391,26.643021042711,2.05806570348264));
#42547=CARTESIAN_POINT('Ctrl Pts',(-24.4520588580831,26.6442600341097,2.05779343180275));
#42548=CARTESIAN_POINT('Ctrl Pts',(-24.4282001298325,26.6511786399603,2.05626065677074));
#42549=CARTESIAN_POINT('Ctrl Pts',(-24.4085306985775,26.6566802664613,2.05499435502827));
#42550=CARTESIAN_POINT('Ctrl Pts',(-24.2683381170094,26.6944596297551,2.04594847663681));
#42551=CARTESIAN_POINT('Ctrl Pts',(-24.1460970596423,26.7198972584676,2.03794781628291));
#42552=CARTESIAN_POINT('Ctrl Pts',(-23.7584308323266,26.7773491101399,2.01221413652531));
#42553=CARTESIAN_POINT('Ctrl Pts',(-23.490355410405,26.7834980069056,1.99380334718602));
#42554=CARTESIAN_POINT('Ctrl Pts',(-23.1219914034802,26.7460857879164,1.9691883103969));
#42555=CARTESIAN_POINT('Ctrl Pts',(-23.0199146007114,26.7307406257783,1.96245715112733));
#42556=CARTESIAN_POINT('Ctrl Pts',(-22.9122619789182,26.7092285118608,1.95557347708528));
#42557=CARTESIAN_POINT('Ctrl Pts',(-22.9057889457377,26.707914305362,1.95516041127388));
#42558=CARTESIAN_POINT('Ctrl Pts',(-22.8968629029976,26.7060734786679,1.95459201663484));
#42559=CARTESIAN_POINT('Ctrl Pts',(-22.8944064573934,26.705563892428,1.95443572067168));
#42560=CARTESIAN_POINT('Ctrl Pts',(-22.8902000522618,26.7046861551426,1.95416829934899));
#42561=CARTESIAN_POINT('Ctrl Pts',(-22.8884498046289,26.7043194160248,1.9540570927335));
#42562=CARTESIAN_POINT('Ctrl Pts',(-22.8850344366407,26.7036008069297,1.95384021641975));
#42563=CARTESIAN_POINT('Ctrl Pts',(-22.8833692941746,26.7032490756889,1.95373453929666));
#42564=CARTESIAN_POINT('Ctrl Pts',(-22.8793409989754,26.7023948372931,1.95347902931546));
#42565=CARTESIAN_POINT('Ctrl Pts',(-22.8769781258753,26.7018909903443,1.95332927410928));
#42566=CARTESIAN_POINT('Ctrl Pts',(-22.8697184968119,26.7003344474774,1.95286952979833));
#42567=CARTESIAN_POINT('Ctrl Pts',(-22.8648235966829,26.6992729864752,1.95256004424274));
#42568=CARTESIAN_POINT('Ctrl Pts',(-22.8120841605379,26.6877076222422,1.94923076499973));
#42569=CARTESIAN_POINT('Ctrl Pts',(-22.7644793674854,26.6761249169372,1.9462720446646));
#42570=CARTESIAN_POINT('Ctrl Pts',(-22.6281962274381,26.6396553728339,1.93788756972047));
#42571=CARTESIAN_POINT('Ctrl Pts',(-22.5402923338682,26.6120462565927,1.93258479790501));
#42572=CARTESIAN_POINT('Ctrl Pts',(-22.3238522786132,26.5337276475404,1.9195241354689));
#42573=CARTESIAN_POINT('Ctrl Pts',(-22.1973892682305,26.478531424086,1.91188432929591));
#42574=CARTESIAN_POINT('Ctrl Pts',(-22.075035775028,26.4155366508264,1.90417269213721));
#42575=CARTESIAN_POINT('',(-26.7730025245988,23.5504663859432,2.06117200133249));
#42576=CARTESIAN_POINT('Ctrl Pts',(-22.0750360931093,26.4155368145933,1.65435918102699));
#42577=CARTESIAN_POINT('Ctrl Pts',(-22.1241974666802,26.4408479737227,1.65763718003993));
#42578=CARTESIAN_POINT('Ctrl Pts',(-22.1740119429965,26.4648947751088,1.66095646117125));
#42579=CARTESIAN_POINT('Ctrl Pts',(-22.2344161870542,26.492158765002,1.66498807657907));
#42580=CARTESIAN_POINT('Ctrl Pts',(-22.2444238915245,26.496614547692,1.66565623777394));
#42581=CARTESIAN_POINT('Ctrl Pts',(-22.2584387265136,26.5027690168378,1.6665922895853));
#42582=CARTESIAN_POINT('Ctrl Pts',(-22.2624269541482,26.504510777653,1.66685870364032));
#42583=CARTESIAN_POINT('Ctrl Pts',(-22.2693286116832,26.5075082762307,1.66731980910595));
#42584=CARTESIAN_POINT('Ctrl Pts',(-22.2722403979568,26.5087678034753,1.66751437067434));
#42585=CARTESIAN_POINT('Ctrl Pts',(-22.2782162902034,26.5113422771571,1.66791372027616));
#42586=CARTESIAN_POINT('Ctrl Pts',(-22.2812805852638,26.5126567713944,1.66811852342681));
#42587=CARTESIAN_POINT('Ctrl Pts',(-22.2884222877264,26.5157072416525,1.66859590509598));
#42588=CARTESIAN_POINT('Ctrl Pts',(-22.2925012394358,26.5174395645444,1.66886860778774));
#42589=CARTESIAN_POINT('Ctrl Pts',(-22.301098561572,26.5210699174754,1.66944349805045));
#42590=CARTESIAN_POINT('Ctrl Pts',(-22.3056177108143,26.5229660636309,1.66974574903111));
#42591=CARTESIAN_POINT('Ctrl Pts',(-22.3177014361431,26.5280037724304,1.67055411087161));
#42592=CARTESIAN_POINT('Ctrl Pts',(-22.3252736566569,26.5311268008594,1.67106085044095));
#42593=CARTESIAN_POINT('Ctrl Pts',(-22.3483201160454,26.5405292603721,1.67260373809438));
#42594=CARTESIAN_POINT('Ctrl Pts',(-22.3638311462971,26.5467172361735,1.67364297168359));
#42595=CARTESIAN_POINT('Ctrl Pts',(-22.6621442879888,26.6630470226429,1.69364751729217));
#42596=CARTESIAN_POINT('Ctrl Pts',(-22.9589992207896,26.7327923065176,1.71407786648253));
#42597=CARTESIAN_POINT('Ctrl Pts',(-23.3942292599906,26.7719964756639,1.74363247458185));
#42598=CARTESIAN_POINT('Ctrl Pts',(-23.5279586530674,26.775696060919,1.75262497783683));
#42599=CARTESIAN_POINT('Ctrl Pts',(-23.6669601883247,26.7708931967524,1.76165985002547));
#42600=CARTESIAN_POINT('Ctrl Pts',(-23.6723794263449,26.770692252122,1.76201158805565));
#42601=CARTESIAN_POINT('Ctrl Pts',(-23.6804115566134,26.7703741181029,1.76253214624319));
#42602=CARTESIAN_POINT('Ctrl Pts',(-23.6830248283657,26.7702674261237,1.76270139006518));
#42603=CARTESIAN_POINT('Ctrl Pts',(-23.731459746752,26.7682309117269,1.76583591361869));
#42604=CARTESIAN_POINT('Ctrl Pts',(-23.7772381995104,26.7653262414096,1.76876080400806));
#42605=CARTESIAN_POINT('Ctrl Pts',(-23.8279069428879,26.7610235325598,1.77194488731095));
#42606=CARTESIAN_POINT('Ctrl Pts',(-23.8328710546547,26.7605903898216,1.77225626951248));
#42607=CARTESIAN_POINT('Ctrl Pts',(-23.8402877999746,26.7599259067,1.77272062742192));
#42608=CARTESIAN_POINT('Ctrl Pts',(-23.8427411758737,26.7597032672864,1.77287408950548));
#42609=CARTESIAN_POINT('Ctrl Pts',(-23.8469630611093,26.7593152576567,1.77313792658219));
#42610=CARTESIAN_POINT('Ctrl Pts',(-23.8487316885717,26.759151238474,1.77324837807625));
#42611=CARTESIAN_POINT('Ctrl Pts',(-23.8523901103427,26.7588089125549,1.77347669187531));
#42612=CARTESIAN_POINT('Ctrl Pts',(-23.8542798794187,26.7586303986923,1.77359454168288));
#42613=CARTESIAN_POINT('Ctrl Pts',(-23.8587252459414,26.7582065117766,1.77387156244463));
#42614=CARTESIAN_POINT('Ctrl Pts',(-23.8612807168373,26.7579597536704,1.77403065463605));
#42615=CARTESIAN_POINT('Ctrl Pts',(-23.8696165116455,26.7571447883298,1.7745491015065));
#42616=CARTESIAN_POINT('Ctrl Pts',(-23.8753956374863,26.7565640042997,1.77490774736355));
#42617=CARTESIAN_POINT('Ctrl Pts',(-24.0170057242009,26.7419458284085,1.78367726898743));
#42618=CARTESIAN_POINT('Ctrl Pts',(-24.1518300673804,26.7193028259447,1.79160809727196));
#42619=CARTESIAN_POINT('Ctrl Pts',(-24.4249212635529,26.6553731242429,1.80754090308574));
#42620=CARTESIAN_POINT('Ctrl Pts',(-24.5626648529085,26.6132319637872,1.81550940469176));
#42621=CARTESIAN_POINT('Ctrl Pts',(-24.7756361188824,26.5321325997473,1.82828423502202));
#42622=CARTESIAN_POINT('Ctrl Pts',(-24.8529363527473,26.4991824495921,1.8330196508188));
#42623=CARTESIAN_POINT('Ctrl Pts',(-25.0585656244851,26.4018663209937,1.84603619954275));
#42624=CARTESIAN_POINT('Ctrl Pts',(-25.1840114563436,26.331894678704,1.85444484685241));
#42625=CARTESIAN_POINT('Ctrl Pts',(-25.3136736328019,26.2477674305825,1.86384665853346));
#42626=CARTESIAN_POINT('Ctrl Pts',(-25.32294789353,26.241681846919,1.86452318141433));
#42627=CARTESIAN_POINT('Ctrl Pts',(-25.3358361859438,26.2331292937447,1.86546906327035));
#42628=CARTESIAN_POINT('Ctrl Pts',(-25.3394769656996,26.230702611648,1.86573690429099));
#42629=CARTESIAN_POINT('Ctrl Pts',(-25.3457541422362,26.2265002094717,1.86619981055906));
#42630=CARTESIAN_POINT('Ctrl Pts',(-25.3483928815189,26.2247279846553,1.86639474354621));
#42631=CARTESIAN_POINT('Ctrl Pts',(-25.3537912016489,26.2210907750093,1.8667942374115));
#42632=CARTESIAN_POINT('Ctrl Pts',(-25.356550520749,26.2192254110213,1.86699881248299));
#42633=CARTESIAN_POINT('Ctrl Pts',(-25.3629565549927,26.2148802982208,1.86747463172042));
#42634=CARTESIAN_POINT('Ctrl Pts',(-25.3666010753379,26.2123973395365,1.8677459976233));
#42635=CARTESIAN_POINT('Ctrl Pts',(-25.3742601441406,26.2071562777888,1.86831768356301));
#42636=CARTESIAN_POINT('Ctrl Pts',(-25.3782735561099,26.2043965406264,1.86861806550848));
#42637=CARTESIAN_POINT('Ctrl Pts',(-25.3889596977429,26.1970127074049,1.86942004781553));
#42638=CARTESIAN_POINT('Ctrl Pts',(-25.3956212047192,26.192372500372,1.86992226389777));
#42639=CARTESIAN_POINT('Ctrl Pts',(-25.415767928832,26.178225532919,1.87144810905059));
#42640=CARTESIAN_POINT('Ctrl Pts',(-25.4291975776097,26.1686404499018,1.87247474411924));
#42641=CARTESIAN_POINT('Ctrl Pts',(-25.5914775779532,26.0509257026233,1.88499782295571));
#42642=CARTESIAN_POINT('Ctrl Pts',(-25.7308522741064,25.9303638848626,1.89699277666627));
#42643=CARTESIAN_POINT('Ctrl Pts',(-26.064470642144,25.5877575811898,1.92899359177089));
#42644=CARTESIAN_POINT('Ctrl Pts',(-26.2399303620716,25.349797395405,1.94942377213292));
#42645=CARTESIAN_POINT('Ctrl Pts',(-26.3881677059003,25.0775382171164,1.96903385076223));
#42646=CARTESIAN_POINT('Ctrl Pts',(-26.3955752751814,25.0636931847023,1.97002130378236));
#42647=CARTESIAN_POINT('Ctrl Pts',(-26.4045310410809,25.0466563276915,1.97122396278808));
#42648=CARTESIAN_POINT('Ctrl Pts',(-26.4061753758983,25.0435156826737,1.97144515061144));
#42649=CARTESIAN_POINT('Ctrl Pts',(-26.4088837466532,25.0383219140542,1.97181007599604));
#42650=CARTESIAN_POINT('Ctrl Pts',(-26.4099507551336,25.0362703582304,1.97195400176455));
#42651=CARTESIAN_POINT('Ctrl Pts',(-26.4117889416649,25.0327267331091,1.97220221923424));
#42652=CARTESIAN_POINT('Ctrl Pts',(-26.4125611601128,25.031235211936,1.97230657737779));
#42653=CARTESIAN_POINT('Ctrl Pts',(-26.4142924996836,25.0278847591941,1.97254073686263));
#42654=CARTESIAN_POINT('Ctrl Pts',(-26.4152509754843,25.0260255003881,1.97267049668115));
#42655=CARTESIAN_POINT('Ctrl Pts',(-26.4178008920491,25.0210673057413,1.97301605412005));
#42656=CARTESIAN_POINT('Ctrl Pts',(-26.4193891250588,25.0179667093932,1.97323164777198));
#42657=CARTESIAN_POINT('Ctrl Pts',(-26.4267789212413,25.0034822938528,1.97423648885563));
#42658=CARTESIAN_POINT('Ctrl Pts',(-26.4325178864234,24.992066406363,1.97502182195642));
#42659=CARTESIAN_POINT('Ctrl Pts',(-26.5690763079747,24.7163519358614,1.99383705143902));
#42660=CARTESIAN_POINT('Ctrl Pts',(-26.6630978776438,24.4353212491886,2.00975184648338));
#42661=CARTESIAN_POINT('Ctrl Pts',(-26.7544403727407,23.9491860270695,2.03758928423975));
#42662=CARTESIAN_POINT('Ctrl Pts',(-26.7729892818748,23.7500321587208,2.04906084790339));
#42663=CARTESIAN_POINT('Ctrl Pts',(-26.7730025245988,23.5504663859432,2.06117200133249));
#42664=CARTESIAN_POINT('Ctrl Pts',(-26.7730025246672,23.5504653522829,2.06117206406279));
#42665=CARTESIAN_POINT('Ctrl Pts',(-26.7730030301775,23.5428103913733,2.06163662479375));
#42666=CARTESIAN_POINT('Ctrl Pts',(-26.7729762615759,23.5351554912076,2.06210202842088));
#42667=CARTESIAN_POINT('Ctrl Pts',(-26.7728668282953,23.5196548135235,2.06304618952845));
#42668=CARTESIAN_POINT('Ctrl Pts',(-26.7727827839904,23.511809114334,2.06352498594758));
#42669=CARTESIAN_POINT('Ctrl Pts',(-26.772614772016,23.500112847161,2.06424014790564));
#42670=CARTESIAN_POINT('Ctrl Pts',(-26.7725525508248,23.4962619554381,2.06447583138215));
#42671=CARTESIAN_POINT('Ctrl Pts',(-26.7724265270868,23.4892414122739,2.06490591453335));
#42672=CARTESIAN_POINT('Ctrl Pts',(-26.7723649500896,23.4860717215934,2.06510024416008));
#42673=CARTESIAN_POINT('Ctrl Pts',(-26.7722357464253,23.479890612096,2.06547949893997));
#42674=CARTESIAN_POINT('Ctrl Pts',(-26.772168574643,23.4768791862025,2.06566440961753));
#42675=CARTESIAN_POINT('Ctrl Pts',(-26.7720173249408,23.4704995935676,2.0660564309928));
#42676=CARTESIAN_POINT('Ctrl Pts',(-26.7719321869442,23.4671314576255,2.06626357477444));
#42677=CARTESIAN_POINT('Ctrl Pts',(-26.7716756398554,23.4575754590055,2.06685177614449));
#42678=CARTESIAN_POINT('Ctrl Pts',(-26.7714916845276,23.4513879728562,2.06723322736863));
#42679=CARTESIAN_POINT('Ctrl Pts',(-26.7705662773994,23.4230135794938,2.06898522331759));
#42680=CARTESIAN_POINT('Ctrl Pts',(-26.7696134331534,23.4008346004517,2.07036239223191));
#42681=CARTESIAN_POINT('Ctrl Pts',(-26.7524925549218,23.0797220527192,2.09041703916769));
#42682=CARTESIAN_POINT('Ctrl Pts',(-26.6949796923149,22.7845191191838,2.11051495921379));
#42683=CARTESIAN_POINT('Ctrl Pts',(-26.5382238389041,22.3290020717458,2.14311126545295));
#42684=CARTESIAN_POINT('Ctrl Pts',(-26.4642778653392,22.161764889373,2.15540449737877));
#42685=CARTESIAN_POINT('Ctrl Pts',(-26.3689169849746,21.9877221193492,2.16795733091916));
#42686=CARTESIAN_POINT('Ctrl Pts',(-26.36117014571,21.9738284828484,2.16895751933203));
#42687=CARTESIAN_POINT('Ctrl Pts',(-26.3514683737279,21.9567276783878,2.17018570240719));
#42688=CARTESIAN_POINT('Ctrl Pts',(-26.3496104693446,21.9534661373944,2.1704198163315));
#42689=CARTESIAN_POINT('Ctrl Pts',(-26.3466784343106,21.9483398110055,2.17078757007863));
#42690=CARTESIAN_POINT('Ctrl Pts',(-26.3456081343642,21.9464728559859,2.17092145727548));
#42691=CARTESIAN_POINT('Ctrl Pts',(-26.3436059964716,21.9429885622767,2.17117124467223));
#42692=CARTESIAN_POINT('Ctrl Pts',(-26.3426746296233,21.9413709718532,2.17128717408809));
#42693=CARTESIAN_POINT('Ctrl Pts',(-26.3405829590522,21.9377454629886,2.1715469294805));
#42694=CARTESIAN_POINT('Ctrl Pts',(-26.3394218956156,21.9357379916791,2.17169070487653));
#42695=CARTESIAN_POINT('Ctrl Pts',(-26.3364698421235,21.9306465982311,2.1720552209492));
#42696=CARTESIAN_POINT('Ctrl Pts',(-26.3346758928518,21.9275643833536,2.17227576928163));
#42697=CARTESIAN_POINT('Ctrl Pts',(-26.3248249072765,21.9107036738795,2.1734816097101));
#42698=CARTESIAN_POINT('Ctrl Pts',(-26.3166705259008,21.8969818851879,2.1744606543097));
#42699=CARTESIAN_POINT('Ctrl Pts',(-26.1463218590701,21.6151171814071,2.19453587248533));
#42700=CARTESIAN_POINT('Ctrl Pts',(-25.9459469521276,21.371938971088,2.21130701930035));
#42701=CARTESIAN_POINT('Ctrl Pts',(-25.5905941411122,21.050122244552,2.23842650704243));
#42702=CARTESIAN_POINT('Ctrl Pts',(-25.4592151151905,20.9484270149588,2.24801405219184));
#42703=CARTESIAN_POINT('Ctrl Pts',(-25.3074308388297,20.8486436632403,2.25897929262195));
#42704=CARTESIAN_POINT('Ctrl Pts',(-25.2941947708239,20.840080667377,2.25993445675901));
#42705=CARTESIAN_POINT('Ctrl Pts',(-25.2742742712252,20.8273995736589,2.26137068151381));
#42706=CARTESIAN_POINT('Ctrl Pts',(-25.2676366186432,20.8232081452492,2.26184902520465));
#42707=CARTESIAN_POINT('Ctrl Pts',(-25.2569504380506,20.8165147116048,2.26261880810875));
#42708=CARTESIAN_POINT('Ctrl Pts',(-25.2529115383619,20.8139973317575,2.2629096789287));
#42709=CARTESIAN_POINT('Ctrl Pts',(-25.2451883699335,20.8092073285982,2.26346574931758));
#42710=CARTESIAN_POINT('Ctrl Pts',(-25.2415050667286,20.8069331620958,2.26373089125598));
#42711=CARTESIAN_POINT('Ctrl Pts',(-25.2349907002316,20.8029291300299,2.26419973103681));
#42712=CARTESIAN_POINT('Ctrl Pts',(-25.2321615208812,20.8011961987287,2.26440331562683));
#42713=CARTESIAN_POINT('Ctrl Pts',(-25.2265957479355,20.7977988548634,2.26480376228176));
#42714=CARTESIAN_POINT('Ctrl Pts',(-25.2238593382915,20.796134146707,2.26500061318987));
#42715=CARTESIAN_POINT('Ctrl Pts',(-25.2173003315207,20.7921573278004,2.26547238703523));
#42716=CARTESIAN_POINT('Ctrl Pts',(-25.2134754067405,20.7898490850476,2.26574745146423));
#42717=CARTESIAN_POINT('Ctrl Pts',(-25.1996623138714,20.7815523748684,2.26674061917723));
#42718=CARTESIAN_POINT('Ctrl Pts',(-25.1896465950827,20.7756101606567,2.26746041062464));
#42719=CARTESIAN_POINT('Ctrl Pts',(-25.0164318900992,20.6741090958042,2.27990352994431));
#42720=CARTESIAN_POINT('Ctrl Pts',(-24.8451964529509,20.5930612703739,2.29215972238692));
#42721=CARTESIAN_POINT('Ctrl Pts',(-24.5765732000631,20.4937416966127,2.31127165786629));
#42722=CARTESIAN_POINT('Ctrl Pts',(-24.4837948118511,20.4641400763565,2.3178464838661));
#42723=CARTESIAN_POINT('Ctrl Pts',(-24.3629448235205,20.4315310276109,2.32631877565821));
#42724=CARTESIAN_POINT('Ctrl Pts',(-24.3359740787569,20.4246271167725,2.32820364717702));
#42725=CARTESIAN_POINT('Ctrl Pts',(-24.135035793073,20.3759565944167,2.34219160710207));
#42726=CARTESIAN_POINT('Ctrl Pts',(-23.9579269078721,20.348386929382,2.35423515292208));
#42727=CARTESIAN_POINT('Ctrl Pts',(-23.7623021109567,20.3344404585691,2.36665353498257));
#42728=CARTESIAN_POINT('Ctrl Pts',(-23.7451673158523,20.3333564233635,2.36773374378712));
#42729=CARTESIAN_POINT('Ctrl Pts',(-23.7241827713985,20.3321971194842,2.36904677632269));
#42730=CARTESIAN_POINT('Ctrl Pts',(-23.7203409126009,20.3319917735538,2.36928676206817));
#42731=CARTESIAN_POINT('Ctrl Pts',(-23.7143288508363,20.3316812268013,2.36966166873918));
#42732=CARTESIAN_POINT('Ctrl Pts',(-23.712158909681,20.3315713408929,2.36979685322604));
#42733=CARTESIAN_POINT('Ctrl Pts',(-23.7083139308726,20.3313805291353,2.37003615616043));
#42734=CARTESIAN_POINT('Ctrl Pts',(-23.7066389504825,20.3312987167394,2.3701403243213));
#42735=CARTESIAN_POINT('Ctrl Pts',(-23.7030501837311,20.331126235511,2.37036334339759));
#42736=CARTESIAN_POINT('Ctrl Pts',(-23.7011363855756,20.3310359661409,2.37048217118767));
#42737=CARTESIAN_POINT('Ctrl Pts',(-23.6955787167573,20.3307787908424,2.37082695198532));
#42738=CARTESIAN_POINT('Ctrl Pts',(-23.6919346266934,20.3306163639932,2.37105265193657));
#42739=CARTESIAN_POINT('Ctrl Pts',(-23.6755008403376,20.3299118209543,2.37206886405149));
#42740=CARTESIAN_POINT('Ctrl Pts',(-23.6627080277553,20.3294397140333,2.37285548144107));
#42741=CARTESIAN_POINT('Ctrl Pts',(-23.6463686288345,20.3289341945299,2.37385488104211));
#42742=CARTESIAN_POINT('Ctrl Pts',(-23.642824570364,20.3288303998719,2.37407133550049));
#42743=CARTESIAN_POINT('Ctrl Pts',(-23.3141547621791,20.3197474984519,2.39411605781885));
#42744=CARTESIAN_POINT('Ctrl Pts',(-22.9894810956702,20.3600291549973,2.41144060698491));
#42745=CARTESIAN_POINT('Ctrl Pts',(-22.5268894787106,20.4903605199775,2.43871206747533));
#42746=CARTESIAN_POINT('Ctrl Pts',(-22.3807405853043,20.543186967019,2.44771408655974));
#42747=CARTESIAN_POINT('Ctrl Pts',(-22.2250494232986,20.6125345806638,2.45800733201461));
#42748=CARTESIAN_POINT('Ctrl Pts',(-22.2111658211919,20.6188370361138,2.45893145772388));
#42749=CARTESIAN_POINT('Ctrl Pts',(-22.1903754059429,20.6284533531939,2.46032492897523));
#42750=CARTESIAN_POINT('Ctrl Pts',(-22.1834346999271,20.6316937692567,2.46079174745395));
#42751=CARTESIAN_POINT('Ctrl Pts',(-22.1722723549476,20.6369536978693,2.46154514523939));
#42752=CARTESIAN_POINT('Ctrl Pts',(-22.168043418693,20.6389577286478,2.46183118822405));
#42753=CARTESIAN_POINT('Ctrl Pts',(-22.1599627298285,20.642808624024,2.46237894163569));
#42754=CARTESIAN_POINT('Ctrl Pts',(-22.1561102520167,20.6446539508235,2.46264059821849));
#42755=CARTESIAN_POINT('Ctrl Pts',(-22.1492797769412,20.6479424424481,2.46310543604126));
#42756=CARTESIAN_POINT('Ctrl Pts',(-22.1463003065786,20.6493825478514,2.46330851039401));
#42757=CARTESIAN_POINT('Ctrl Pts',(-22.1404237765402,20.6522341002824,2.46370965860968));
#42758=CARTESIAN_POINT('Ctrl Pts',(-22.1375266047444,20.6536453089492,2.46390772397547));
#42759=CARTESIAN_POINT('Ctrl Pts',(-22.1305527763274,20.6570552032996,2.46438520725713));
#42760=CARTESIAN_POINT('Ctrl Pts',(-22.126478225148,20.6590581591019,2.4646647744041));
#42761=CARTESIAN_POINT('Ctrl Pts',(-22.1139728333184,20.6652383689544,2.46552463365017));
#42762=CARTESIAN_POINT('Ctrl Pts',(-22.1055560994646,20.6694439113823,2.46610591708006));
#42763=CARTESIAN_POINT('Ctrl Pts',(-22.006785077225,20.7193379931196,2.4729577238437));
#42764=CARTESIAN_POINT('Ctrl Pts',(-21.918623014948,20.7692184950627,2.47937635083919));
#42765=CARTESIAN_POINT('Ctrl Pts',(-21.6614196796813,20.9311833164757,2.49906375337599));
#42766=CARTESIAN_POINT('Ctrl Pts',(-21.5004726790975,21.0551381122436,2.51273749521673));
#42767=CARTESIAN_POINT('Ctrl Pts',(-21.3282386234179,21.2157611491492,2.52867861130471));
#42768=CARTESIAN_POINT('Ctrl Pts',(-21.3045676599009,21.2385225947048,2.53090048542475));
#42769=CARTESIAN_POINT('Ctrl Pts',(-21.2537257234002,21.2889289652941,2.53573575801697));
#42770=CARTESIAN_POINT('Ctrl Pts',(-21.2266969042811,21.3167107269738,2.5383471756131));
#42771=CARTESIAN_POINT('Ctrl Pts',(-21.1107874413812,21.440230787809,2.54970701746402));
#42772=CARTESIAN_POINT('Ctrl Pts',(-21.0272614401654,21.540847990174,2.55832389388032));
#42773=CARTESIAN_POINT('Ctrl Pts',(-20.945328457863,21.6527403625358,2.56703179843677));
#42774=CARTESIAN_POINT('Ctrl Pts',(-20.9406151416111,21.6592277941297,2.56753369910608));
#42775=CARTESIAN_POINT('Ctrl Pts',(-20.9342159169173,21.6681052087411,2.56821637260278));
#42776=CARTESIAN_POINT('Ctrl Pts',(-20.9325090270918,21.670479923258,2.56839858695983));
#42777=CARTESIAN_POINT('Ctrl Pts',(-20.9296589142607,21.6744565598987,2.56870304324721));
#42778=CARTESIAN_POINT('Ctrl Pts',(-20.9285139262551,21.6760572056042,2.56882540808877));
#42779=CARTESIAN_POINT('Ctrl Pts',(-20.9262621228596,21.6792112347541,2.56906616371359));
#42780=CARTESIAN_POINT('Ctrl Pts',(-20.925155220334,21.6807645519431,2.56918456047483));
#42781=CARTESIAN_POINT('Ctrl Pts',(-20.9227180609442,21.6841910520281,2.5694453576293));
#42782=CARTESIAN_POINT('Ctrl Pts',(-20.9213884244894,21.6860646798938,2.56958771481183));
#42783=CARTESIAN_POINT('Ctrl Pts',(-20.9167524946352,21.6926121215739,2.57008432632749));
#42784=CARTESIAN_POINT('Ctrl Pts',(-20.9134566274837,21.6972933580386,2.57043786253606));
#42785=CARTESIAN_POINT('Ctrl Pts',(-20.8803360274832,21.7446030322833,2.57399567977419));
#42786=CARTESIAN_POINT('Ctrl Pts',(-20.8515331255406,21.787941951208,2.57713149454015));
#42787=CARTESIAN_POINT('Ctrl Pts',(-20.6486561715143,22.1098528441634,2.599683805621));
#42788=CARTESIAN_POINT('Ctrl Pts',(-20.5170149165162,22.4129120544996,2.61712865174157));
#42789=CARTESIAN_POINT('Ctrl Pts',(-20.4036561779065,22.8440081789899,2.64277107258762));
#42790=CARTESIAN_POINT('Ctrl Pts',(-20.380061580497,22.9588691076529,2.64965452512963));
#42791=CARTESIAN_POINT('Ctrl Pts',(-20.3608589551612,23.0875920324066,2.65753040407917));
#42792=CARTESIAN_POINT('Ctrl Pts',(-20.3590209950157,23.1004443555903,2.65831848385404));
#42793=CARTESIAN_POINT('Ctrl Pts',(-20.3563375601448,23.1200536444074,2.65952362829603));
#42794=CARTESIAN_POINT('Ctrl Pts',(-20.355435743757,23.1268028670266,2.65993891485386));
#42795=CARTESIAN_POINT('Ctrl Pts',(-20.353996421507,23.1378411769629,2.66061893905677));
#42796=CARTESIAN_POINT('Ctrl Pts',(-20.3534461402716,23.142128600893,2.6608832728024));
#42797=CARTESIAN_POINT('Ctrl Pts',(-20.3524020011353,23.1503955234636,2.66139335310589));
#42798=CARTESIAN_POINT('Ctrl Pts',(-20.3519069413694,23.1543748644296,2.66163906120622));
#42799=CARTESIAN_POINT('Ctrl Pts',(-20.3510203938014,23.1616112421496,2.66208620433249));
#42800=CARTESIAN_POINT('Ctrl Pts',(-20.3506264489566,23.1648679775022,2.66228756139004));
#42801=CARTESIAN_POINT('Ctrl Pts',(-20.3498416541829,23.1714400165466,2.66269414114037));
#42802=CARTESIAN_POINT('Ctrl Pts',(-20.3494509816387,23.1747553365586,2.66289936914962));
#42803=CARTESIAN_POINT('Ctrl Pts',(-20.3483683114657,23.1840675451735,2.6634761775757));
#42804=CARTESIAN_POINT('Ctrl Pts',(-20.3476880139432,23.1900657566035,2.66384812724026));
#42805=CARTESIAN_POINT('Ctrl Pts',(-20.3449748466093,23.2146033605156,2.66537142463432));
#42806=CARTESIAN_POINT('Ctrl Pts',(-20.343086109648,23.233158030996,2.66652731294229));
#42807=CARTESIAN_POINT('Ctrl Pts',(-20.3046911596426,23.6458719081593,2.69233061086009));
#42808=CARTESIAN_POINT('Ctrl Pts',(-20.3409731505091,24.0433509332076,2.71968110425252));
#42809=CARTESIAN_POINT('Ctrl Pts',(-20.4563424003248,24.4528761343452,2.74795188633107));
#42810=CARTESIAN_POINT('Ctrl Pts',(-20.4648389525128,24.4815056715679,2.74992542968048));
#42811=CARTESIAN_POINT('Ctrl Pts',(-20.4935601456592,24.5735716244023,2.75625442161755));
#42812=CARTESIAN_POINT('Ctrl Pts',(-20.5153544236156,24.6365053931723,2.76055393774446));
#42813=CARTESIAN_POINT('Ctrl Pts',(-20.5429388351263,24.7088287525354,2.76542774359601));
#42814=CARTESIAN_POINT('Ctrl Pts',(-20.5468438554051,24.7189145273974,2.7661058667078));
#42815=CARTESIAN_POINT('Ctrl Pts',(-20.5519992655365,24.7320332525235,2.766985710748));
#42816=CARTESIAN_POINT('Ctrl Pts',(-20.5532035568981,24.7350840653105,2.76719016640146));
#42817=CARTESIAN_POINT('Ctrl Pts',(-20.5551666911704,24.7400350987923,2.76752170954256));
#42818=CARTESIAN_POINT('Ctrl Pts',(-20.5559226861174,24.7419364348419,2.76764896927596));
#42819=CARTESIAN_POINT('Ctrl Pts',(-20.5573797961917,24.7455909426591,2.76789345048418));
#42820=CARTESIAN_POINT('Ctrl Pts',(-20.5580806393164,24.7473442132794,2.76801068771679));
#42821=CARTESIAN_POINT('Ctrl Pts',(-20.5596988616986,24.7513821544456,2.76828057298727));
#42822=CARTESIAN_POINT('Ctrl Pts',(-20.5606173207568,24.7536663962459,2.76843315517611));
#42823=CARTESIAN_POINT('Ctrl Pts',(-20.5630806258084,24.7597725027112,2.76884079296712));
#42824=CARTESIAN_POINT('Ctrl Pts',(-20.5646301951342,24.7635924756031,2.76909556283772));
#42825=CARTESIAN_POINT('Ctrl Pts',(-20.5717939282391,24.7811555747387,2.77026582405475));
#42826=CARTESIAN_POINT('Ctrl Pts',(-20.577495798041,24.7948630636545,2.77117609056848));
#42827=CARTESIAN_POINT('Ctrl Pts',(-20.7098117686798,25.1068577774496,2.79183462953358));
#42828=CARTESIAN_POINT('Ctrl Pts',(-20.8806242649835,25.3844533162252,2.80910307819126));
#42829=CARTESIAN_POINT('Ctrl Pts',(-21.1909254291394,25.751183490686,2.83635444299253));
#42830=CARTESIAN_POINT('Ctrl Pts',(-21.300355331277,25.8629294103558,2.84541121905516));
#42831=CARTESIAN_POINT('Ctrl Pts',(-21.4289141943782,25.9764172513883,2.85576724678622));
#42832=CARTESIAN_POINT('Ctrl Pts',(-21.4404545586771,25.9864594377371,2.85669441816827));
#42833=CARTESIAN_POINT('Ctrl Pts',(-21.4578941580385,26.0014181646639,2.85809208796558));
#42834=CARTESIAN_POINT('Ctrl Pts',(-21.4637402927719,26.0063965012704,2.85856004100092));
#42835=CARTESIAN_POINT('Ctrl Pts',(-21.4731838731496,26.0143802320581,2.85931505224242));
#42836=CARTESIAN_POINT('Ctrl Pts',(-21.4767702059011,26.017398773867,2.85960157100954));
#42837=CARTESIAN_POINT('Ctrl Pts',(-21.4836416223597,26.0231567369024,2.86015015210447));
#42838=CARTESIAN_POINT('Ctrl Pts',(-21.4869256015698,26.0258974654156,2.860412160235));
#42839=CARTESIAN_POINT('Ctrl Pts',(-21.4927605425126,26.0307474890549,2.86087739877659));
#42840=CARTESIAN_POINT('Ctrl Pts',(-21.4953093207737,26.0328594113266,2.86108052165847));
#42841=CARTESIAN_POINT('Ctrl Pts',(-21.5003444072504,26.0370184266232,2.86148159538987));
#42842=CARTESIAN_POINT('Ctrl Pts',(-21.5028305398763,26.0390657272043,2.8616795374749));
#42843=CARTESIAN_POINT('Ctrl Pts',(-21.5095300563892,26.0445658672728,2.8622126962302));
#42844=CARTESIAN_POINT('Ctrl Pts',(-21.5137491190402,26.0480117448543,2.86254819459288));
#42845=CARTESIAN_POINT('Ctrl Pts',(-21.5292425432874,26.0606004942123,2.86377928658282));
#42846=CARTESIAN_POINT('Ctrl Pts',(-21.5405697723922,26.0696777562319,2.86467752109661));
#42847=CARTESIAN_POINT('Ctrl Pts',(-21.7151238194768,26.2076333453132,2.87849298664016));
#42848=CARTESIAN_POINT('Ctrl Pts',(-21.8903085799789,26.3204282477399,2.89205552908989));
#42849=CARTESIAN_POINT('Ctrl Pts',(-22.0750360171757,26.4155367754983,2.90599376073416));
#42850=CARTESIAN_POINT('Origin',(-23.5502525316942,23.5502525316942,-77.3107734492734));
#42851=CARTESIAN_POINT('',(-22.07503587195,26.4155367007276,4.4051257859302));
#42852=CARTESIAN_POINT('',(-22.075036015346,26.4155367745563,4.16020796448762));
#42853=CARTESIAN_POINT('',(-22.0750360153461,26.4155367745563,-77.3107734492734));
#42854=CARTESIAN_POINT('',(-26.7730023558368,23.5513171860199,3.55804726516272));
#42855=CARTESIAN_POINT('Ctrl Pts',(-22.07503587195,26.4155367007276,4.4051257859302));
#42856=CARTESIAN_POINT('Ctrl Pts',(-21.9684851210008,26.3606781130149,4.39712134444059));
#42857=CARTESIAN_POINT('Ctrl Pts',(-21.8650503536945,26.299904915894,4.38899729673905));
#42858=CARTESIAN_POINT('Ctrl Pts',(-21.6097021045929,26.1300336496419,4.36824558262081));
#42859=CARTESIAN_POINT('Ctrl Pts',(-21.4634532864716,26.0132371846066,4.35566622781161));
#42860=CARTESIAN_POINT('Ctrl Pts',(-21.3196323257045,25.8763197794498,4.34314960938032));
#42861=CARTESIAN_POINT('Ctrl Pts',(-21.3111748571215,25.8681797354251,4.34241305214061));
#42862=CARTESIAN_POINT('Ctrl Pts',(-21.3002339817327,25.8575337300395,4.34145977720384));
#42863=CARTESIAN_POINT('Ctrl Pts',(-21.2977100907245,25.8550697815696,4.34123984077774));
#42864=CARTESIAN_POINT('Ctrl Pts',(-21.2938388617877,25.8512780619603,4.34090245515943));
#42865=CARTESIAN_POINT('Ctrl Pts',(-21.2924886495425,25.8499532498686,4.34078477391695));
#42866=CARTESIAN_POINT('Ctrl Pts',(-21.2898779221846,25.8473871200297,4.34055721622731));
#42867=CARTESIAN_POINT('Ctrl Pts',(-21.2886172691984,25.8461459594713,4.34044732879512));
#42868=CARTESIAN_POINT('Ctrl Pts',(-21.2857921135897,25.8433599019775,4.34020105505616));
#42869=CARTESIAN_POINT('Ctrl Pts',(-21.2842281731215,25.8418144451571,4.34006471430313));
#42870=CARTESIAN_POINT('Ctrl Pts',(-21.2809866800725,25.8386046989011,4.33978210578601));
#42871=CARTESIAN_POINT('Ctrl Pts',(-21.2793093731152,25.8369401616702,4.33963585774823));
#42872=CARTESIAN_POINT('Ctrl Pts',(-21.2750157536095,25.8326698470069,4.33926145059907));
#42873=CARTESIAN_POINT('Ctrl Pts',(-21.2724020770472,25.8300614061775,4.33903350043176));
#42874=CARTESIAN_POINT('Ctrl Pts',(-21.2648491378509,25.8224976419483,4.33837465183869));
#42875=CARTESIAN_POINT('Ctrl Pts',(-21.2599214835365,25.8175306808459,4.33794465512693));
#42876=CARTESIAN_POINT('Ctrl Pts',(-21.1331400584974,25.688902847659,4.32687620605352));
#42877=CARTESIAN_POINT('Ctrl Pts',(-21.0214404109597,25.5555918889305,4.31699183600734));
#42878=CARTESIAN_POINT('Ctrl Pts',(-20.8041232857785,25.2490020483835,4.29588819625619));
#42879=CARTESIAN_POINT('Ctrl Pts',(-20.7030114081795,25.0734698692578,4.28474389514435));
#42880=CARTESIAN_POINT('Ctrl Pts',(-20.5949945918379,24.837072816971,4.26978152398265));
#42881=CARTESIAN_POINT('Ctrl Pts',(-20.5724004535619,24.7838863563566,4.26642060069734));
#42882=CARTESIAN_POINT('Ctrl Pts',(-20.5440076603403,24.711717361796,4.26184987537096));
#42883=CARTESIAN_POINT('Ctrl Pts',(-20.5369360855625,24.6932454228964,4.26067912160974));
#42884=CARTESIAN_POINT('Ctrl Pts',(-20.5276103885707,24.6681972219883,4.25908982367172));
#42885=CARTESIAN_POINT('Ctrl Pts',(-20.5252067603137,24.6616768142737,4.25867594853426));
#42886=CARTESIAN_POINT('Ctrl Pts',(-20.5221894204981,24.6534092684354,4.25815095405821));
#42887=CARTESIAN_POINT('Ctrl Pts',(-20.521556087151,24.6516692729848,4.25804045081151));
#42888=CARTESIAN_POINT('Ctrl Pts',(-20.5185441137583,24.6433720522773,4.25751345205367));
#42889=CARTESIAN_POINT('Ctrl Pts',(-20.5161852798953,24.6368076973906,4.25709633574458));
#42890=CARTESIAN_POINT('Ctrl Pts',(-20.5119734188067,24.6249659257006,4.25634352337775));
#42891=CARTESIAN_POINT('Ctrl Pts',(-20.5101127794223,24.6196912317304,4.2560080707186));
#42892=CARTESIAN_POINT('Ctrl Pts',(-20.5040679124226,24.6024114822052,4.25490869634127));
#42893=CARTESIAN_POINT('Ctrl Pts',(-20.4999410276381,24.5903866158622,4.25414295294901));
#42894=CARTESIAN_POINT('Ctrl Pts',(-20.488831665434,24.5573815022274,4.25203903651663));
#42895=CARTESIAN_POINT('Ctrl Pts',(-20.4819938869267,24.5363536089928,4.25069623500844));
#42896=CARTESIAN_POINT('Ctrl Pts',(-20.4734405716673,24.5090994333402,4.24895223588301));
#42897=CARTESIAN_POINT('Ctrl Pts',(-20.4715264950855,24.5029356945091,4.24855758112382));
#42898=CARTESIAN_POINT('Ctrl Pts',(-20.4685141847668,24.4931315177131,4.24792944519452));
#42899=CARTESIAN_POINT('Ctrl Pts',(-20.4674038493248,24.4894947915054,4.2476963617164));
#42900=CARTESIAN_POINT('Ctrl Pts',(-20.4653365630964,24.4826805672332,4.24725946497918));
#42901=CARTESIAN_POINT('Ctrl Pts',(-20.4643780779643,24.4795035367812,4.24705570236491));
#42902=CARTESIAN_POINT('Ctrl Pts',(-20.4622310020416,24.4723468032983,4.24659654559194));
#42903=CARTESIAN_POINT('Ctrl Pts',(-20.4610451958679,24.4683662770125,4.24634106058987));
#42904=CARTESIAN_POINT('Ctrl Pts',(-20.4575769820611,24.4566413513681,4.24558819545308));
#42905=CARTESIAN_POINT('Ctrl Pts',(-20.4553159905501,24.4488906969849,4.24509011573967));
#42906=CARTESIAN_POINT('Ctrl Pts',(-20.438233076246,24.3895014277996,4.24127037577921));
#42907=CARTESIAN_POINT('Ctrl Pts',(-20.4246761108608,24.3375106057971,4.23790770460332));
#42908=CARTESIAN_POINT('Ctrl Pts',(-20.3834777317323,24.161617708331,4.2264589136504));
#42909=CARTESIAN_POINT('Ctrl Pts',(-20.3618602941651,24.0364400183458,4.21818605949086));
#42910=CARTESIAN_POINT('Ctrl Pts',(-20.3141832127796,23.6123898454376,4.18981716201159));
#42911=CARTESIAN_POINT('Ctrl Pts',(-20.3224236973037,23.3112574914066,4.16896285271615));
#42912=CARTESIAN_POINT('Ctrl Pts',(-20.3777811622714,22.9821932268002,4.14755649513074));
#42913=CARTESIAN_POINT('Ctrl Pts',(-20.3839300920827,22.9488638059815,4.14540655713465));
#42914=CARTESIAN_POINT('Ctrl Pts',(-20.3916035921698,22.9106587453462,4.14296792047436));
#42915=CARTESIAN_POINT('Ctrl Pts',(-20.3926150382862,22.9056838419814,4.14265087683941));
#42916=CARTESIAN_POINT('Ctrl Pts',(-20.3941278801229,22.8983317941206,4.14218310997013));
#42917=CARTESIAN_POINT('Ctrl Pts',(-20.3946202088096,22.8959528242252,4.14203186947006));
#42918=CARTESIAN_POINT('Ctrl Pts',(-20.3954851614186,22.8917969918221,4.14176787778324));
#42919=CARTESIAN_POINT('Ctrl Pts',(-20.39585659676,22.8900198876365,4.14165505799729));
#42920=CARTESIAN_POINT('Ctrl Pts',(-20.3966447607644,22.8862648243074,4.14141681068948));
#42921=CARTESIAN_POINT('Ctrl Pts',(-20.3970618477952,22.8842869474058,4.14129140439968));
#42922=CARTESIAN_POINT('Ctrl Pts',(-20.3981531259212,22.879135983253,4.14096502576443));
#42923=CARTESIAN_POINT('Ctrl Pts',(-20.3988302496512,22.8759635091456,4.14076422272315));
#42924=CARTESIAN_POINT('Ctrl Pts',(-20.4003200114453,22.8690349092924,4.14032612949517));
#42925=CARTESIAN_POINT('Ctrl Pts',(-20.4011345817016,22.8652791974783,4.14008894959252));
#42926=CARTESIAN_POINT('Ctrl Pts',(-20.403535695419,22.8543032786062,4.13939663259931));
#42927=CARTESIAN_POINT('Ctrl Pts',(-20.4051403790128,22.84708700345,4.13894251211326));
#42928=CARTESIAN_POINT('Ctrl Pts',(-20.4107352579961,22.8223291322585,4.13738791756104));
#42929=CARTESIAN_POINT('Ctrl Pts',(-20.414847575211,22.8048150899971,4.13629407866138));
#42930=CARTESIAN_POINT('Ctrl Pts',(-20.4323282254214,22.7330713749046,4.13183415891107));
#42931=CARTESIAN_POINT('Ctrl Pts',(-20.4469592925563,22.6791561593652,4.1285315097568));
#42932=CARTESIAN_POINT('Ctrl Pts',(-20.4863502278237,22.5476296834416,4.12053489419163));
#42933=CARTESIAN_POINT('Ctrl Pts',(-20.5126652626464,22.4705234320225,4.11589905343451));
#42934=CARTESIAN_POINT('Ctrl Pts',(-20.6273990060186,22.1718778154147,4.09786403039087));
#42935=CARTESIAN_POINT('Ctrl Pts',(-20.7373632809484,21.95945338386,4.08479978116152));
#42936=CARTESIAN_POINT('Ctrl Pts',(-20.8873526593137,21.7347397811048,4.06913506552769));
#42937=CARTESIAN_POINT('Ctrl Pts',(-20.9053373533079,21.7086375101815,4.06728586882316));
#42938=CARTESIAN_POINT('Ctrl Pts',(-20.9284729601965,21.6760974736276,4.06494027841518));
#42939=CARTESIAN_POINT('Ctrl Pts',(-20.9332678221882,21.6694079523006,4.06445589723153));
#42940=CARTESIAN_POINT('Ctrl Pts',(-20.9791092032794,21.6059673015754,4.05984113137371));
#42941=CARTESIAN_POINT('Ctrl Pts',(-21.021967270049,21.5505536607487,4.05564856578748));
#42942=CARTESIAN_POINT('Ctrl Pts',(-21.0725578158683,21.4893706712781,4.05081316189486));
#42943=CARTESIAN_POINT('Ctrl Pts',(-21.0785528926741,21.4821843415746,4.05024188664841));
#42944=CARTESIAN_POINT('Ctrl Pts',(-21.0874323582364,21.4716342432703,4.04939824787638));
#42945=CARTESIAN_POINT('Ctrl Pts',(-21.0902925566819,21.4682501021116,4.04912687738053));
#42946=CARTESIAN_POINT('Ctrl Pts',(-21.0953554119298,21.4622848097421,4.04864718207597));
#42947=CARTESIAN_POINT('Ctrl Pts',(-21.097555187782,21.459701213126,4.04843897620356));
#42948=CARTESIAN_POINT('Ctrl Pts',(-21.1021140503072,21.4543640122092,4.0480079343413));
#42949=CARTESIAN_POINT('Ctrl Pts',(-21.1044737110849,21.4516109065842,4.0477850747729));
#42950=CARTESIAN_POINT('Ctrl Pts',(-21.1105313211834,21.4445673557242,4.04721358821548));
#42951=CARTESIAN_POINT('Ctrl Pts',(-21.114235933065,21.4402826798093,4.04686468499379));
#42952=CARTESIAN_POINT('Ctrl Pts',(-21.1294318728703,21.4228007416184,4.04543593150143));
#42953=CARTESIAN_POINT('Ctrl Pts',(-21.1410191349093,21.409687605871,4.04435208342417));
#42954=CARTESIAN_POINT('Ctrl Pts',(-21.2177784248951,21.3242330451534,4.0372077587366));
#42955=CARTESIAN_POINT('Ctrl Pts',(-21.2860873457146,21.2547894112365,4.03101390739717));
#42956=CARTESIAN_POINT('Ctrl Pts',(-21.4903735151517,21.0651112409568,4.01291800140255));
#42957=CARTESIAN_POINT('Ctrl Pts',(-21.6334889245438,20.9531326171695,4.00071755043467));
#42958=CARTESIAN_POINT('Ctrl Pts',(-21.9160373219171,20.7681859456528,3.97786067675297));
#42959=CARTESIAN_POINT('Ctrl Pts',(-22.0528940420453,20.6921976794464,3.96726058667305));
#42960=CARTESIAN_POINT('Ctrl Pts',(-22.2531088857047,20.5993753504602,3.95283875703214));
#42961=CARTESIAN_POINT('Ctrl Pts',(-22.3122874870389,20.574063401569,3.94870341620471));
#42962=CARTESIAN_POINT('Ctrl Pts',(-22.3777028458145,20.548373139294,3.94430014551669));
#42963=CARTESIAN_POINT('Ctrl Pts',(-22.3832225705398,20.5462229507032,3.94392988749525));
#42964=CARTESIAN_POINT('Ctrl Pts',(-22.3909814932393,20.5432251035114,3.94341126529258));
#42965=CARTESIAN_POINT('Ctrl Pts',(-22.3932157117843,20.5423647193068,3.94326213928935));
#42966=CARTESIAN_POINT('Ctrl Pts',(-22.3970922156404,20.5408768591062,3.94300376979348));
#42967=CARTESIAN_POINT('Ctrl Pts',(-22.3987340553236,20.5402482373622,3.94289445691381));
#42968=CARTESIAN_POINT('Ctrl Pts',(-22.4021257119771,20.5389528330951,3.94266888269686));
#42969=CARTESIAN_POINT('Ctrl Pts',(-22.4038755940033,20.5382862327983,3.94255263284976));
#42970=CARTESIAN_POINT('Ctrl Pts',(-22.4080210920587,20.5367111822111,3.94227754625223));
#42971=CARTESIAN_POINT('Ctrl Pts',(-22.4104172191541,20.5358040602268,3.94211879007372));
#42972=CARTESIAN_POINT('Ctrl Pts',(-22.4154989600927,20.5338871482635,3.94178261340583));
#42973=CARTESIAN_POINT('Ctrl Pts',(-22.4181848482057,20.5328780844679,3.94160523655475));
#42974=CARTESIAN_POINT('Ctrl Pts',(-22.425472555509,20.5301512593923,3.9411247715975));
#42975=CARTESIAN_POINT('Ctrl Pts',(-22.4300769832063,20.5284404212048,3.94082209318514));
#42976=CARTESIAN_POINT('Ctrl Pts',(-22.4443837040294,20.5231617564884,3.93988430692415));
#42977=CARTESIAN_POINT('Ctrl Pts',(-22.4540993800933,20.5196300378459,3.93925128580627));
#42978=CARTESIAN_POINT('Ctrl Pts',(-22.4905488350806,20.5065786098205,3.93689015261329));
#42979=CARTESIAN_POINT('Ctrl Pts',(-22.517391853552,20.4973650771939,3.93517885809896));
#42980=CARTESIAN_POINT('Ctrl Pts',(-22.6102952913908,20.466842807378,3.92933926934609));
#42981=CARTESIAN_POINT('Ctrl Pts',(-22.6769237678563,20.4473130673509,3.92529484949624));
#42982=CARTESIAN_POINT('Ctrl Pts',(-23.1186401387562,20.333197494506,3.89910780465876));
#42983=CARTESIAN_POINT('Ctrl Pts',(-23.5074825751874,20.3046496393114,3.87854463488742));
#42984=CARTESIAN_POINT('Ctrl Pts',(-23.9120893949128,20.3478169068271,3.85393246679386));
#42985=CARTESIAN_POINT('Ctrl Pts',(-23.9320125810545,20.3501308022241,3.85271355764969));
#42986=CARTESIAN_POINT('Ctrl Pts',(-23.9580775243418,20.3534048742732,3.85110933089652));
#42987=CARTESIAN_POINT('Ctrl Pts',(-23.9642402348993,20.3541970956721,3.85072933160547));
#42988=CARTESIAN_POINT('Ctrl Pts',(-23.9737455646093,20.3554469670412,3.85014212801616));
#42989=CARTESIAN_POINT('Ctrl Pts',(-23.977089844355,20.3558920552845,3.84993532169187));
#42990=CARTESIAN_POINT('Ctrl Pts',(-23.9837469936487,20.356788692384,3.84952323216202));
#42991=CARTESIAN_POINT('Ctrl Pts',(-23.9870598718346,20.3572401469715,3.84931795218181));
#42992=CARTESIAN_POINT('Ctrl Pts',(-23.9944005023008,20.3582521119411,3.84886263443916));
#42993=CARTESIAN_POINT('Ctrl Pts',(-23.9984279034157,20.3588150913802,3.84861251870254));
#42994=CARTESIAN_POINT('Ctrl Pts',(-24.0100398701518,20.3604607103131,3.84789048079409));
#42995=CARTESIAN_POINT('Ctrl Pts',(-24.0176216161271,20.361562769794,3.84741794331726));
#42996=CARTESIAN_POINT('Ctrl Pts',(-24.0685830859848,20.3691560325501,3.8442342426152));
#42997=CARTESIAN_POINT('Ctrl Pts',(-24.1118285328456,20.3765049694885,3.84149595049705));
#42998=CARTESIAN_POINT('Ctrl Pts',(-24.2275980481276,20.3986184933433,3.83406210437802));
#42999=CARTESIAN_POINT('Ctrl Pts',(-24.2997822557187,20.4150016902376,3.82931655180012));
#43000=CARTESIAN_POINT('Ctrl Pts',(-24.536687018817,20.4774192998406,3.81337190791578));
#43001=CARTESIAN_POINT('Ctrl Pts',(-24.6982932825663,20.534071529534,3.80187534108136));
#43002=CARTESIAN_POINT('Ctrl Pts',(-24.9258808465114,20.6348046722321,3.78503158142683));
#43003=CARTESIAN_POINT('Ctrl Pts',(-24.9959692541866,20.6689172622727,3.77975163361922));
#43004=CARTESIAN_POINT('Ctrl Pts',(-25.1843308531128,20.7691992530821,3.76539858719322));
#43005=CARTESIAN_POINT('Ctrl Pts',(-25.2997914380041,20.8403462535412,3.75641387261008));
#43006=CARTESIAN_POINT('Ctrl Pts',(-25.4222685305741,20.9269181275548,3.74693620850097));
#43007=CARTESIAN_POINT('Ctrl Pts',(-25.4340384464264,20.9353571337317,3.74602604181142));
#43008=CARTESIAN_POINT('Ctrl Pts',(-25.4488056307422,20.9460966309731,3.74488530647954));
#43009=CARTESIAN_POINT('Ctrl Pts',(-25.451856037607,20.948323260593,3.7446497342712));
#43010=CARTESIAN_POINT('Ctrl Pts',(-25.4566607860887,20.9518434259396,3.74427879331534));
#43011=CARTESIAN_POINT('Ctrl Pts',(-25.4584177292043,20.9531333791771,3.74414317592467));
#43012=CARTESIAN_POINT('Ctrl Pts',(-25.461530568216,20.9554236994271,3.74390294211603));
#43013=CARTESIAN_POINT('Ctrl Pts',(-25.4628869811644,20.9564233421784,3.74379827587307));
#43014=CARTESIAN_POINT('Ctrl Pts',(-25.4659813602872,20.9587075700112,3.74355953549685));
#43015=CARTESIAN_POINT('Ctrl Pts',(-25.4677188153151,20.9599928373065,3.74342551025365));
#43016=CARTESIAN_POINT('Ctrl Pts',(-25.4725554609694,20.9635782371367,3.74305248128033));
#43017=CARTESIAN_POINT('Ctrl Pts',(-25.4756518276613,20.9658822003594,3.74281374583492));
#43018=CARTESIAN_POINT('Ctrl Pts',(-25.4825525205745,20.9710361951404,3.74228183586311));
#43019=CARTESIAN_POINT('Ctrl Pts',(-25.4863547044549,20.9738890994357,3.74198886030146));
#43020=CARTESIAN_POINT('Ctrl Pts',(-25.4980453900141,20.9827015026518,3.741088298431));
#43021=CARTESIAN_POINT('Ctrl Pts',(-25.5059128809542,20.9886889642956,3.74048261036278));
#43022=CARTESIAN_POINT('Ctrl Pts',(-25.5349278253085,21.0109820426369,3.73824969656118));
#43023=CARTESIAN_POINT('Ctrl Pts',(-25.5559005821179,21.0275146065447,3.73663734082592));
#43024=CARTESIAN_POINT('Ctrl Pts',(-25.6293475401673,21.0869069150594,3.73098706078739));
#43025=CARTESIAN_POINT('Ctrl Pts',(-25.6806761207035,21.1311609133904,3.72703126809774));
#43026=CARTESIAN_POINT('Ctrl Pts',(-26.0191739760883,21.4421414335047,3.70059742564631));
#43027=CARTESIAN_POINT('Ctrl Pts',(-26.2569881571294,21.7576765512726,3.67980724021613));
#43028=CARTESIAN_POINT('Ctrl Pts',(-26.4410085701265,22.12546495894,3.65492068913603));
#43029=CARTESIAN_POINT('Ctrl Pts',(-26.4494897027726,22.1428031003409,3.65374739229731));
#43030=CARTESIAN_POINT('Ctrl Pts',(-26.4604540219324,22.1657373456577,3.65219490092532));
#43031=CARTESIAN_POINT('Ctrl Pts',(-26.4630778566817,22.1712660780096,3.65182060606667));
#43032=CARTESIAN_POINT('Ctrl Pts',(-26.4671156799694,22.1798371960958,3.65124027172663));
#43033=CARTESIAN_POINT('Ctrl Pts',(-26.4685407019315,22.1828743933849,3.65103461520077));
#43034=CARTESIAN_POINT('Ctrl Pts',(-26.4713771676027,22.1889444789014,3.65062356434448));
#43035=CARTESIAN_POINT('Ctrl Pts',(-26.4727886368106,22.1919773507137,3.65041817121054));
#43036=CARTESIAN_POINT('Ctrl Pts',(-26.4759188952197,22.1987309115799,3.64996076900529));
#43037=CARTESIAN_POINT('Ctrl Pts',(-26.4776353118819,22.2024526881292,3.64970867832266));
#43038=CARTESIAN_POINT('Ctrl Pts',(-26.482602693946,22.2132779184763,3.64897536726457));
#43039=CARTESIAN_POINT('Ctrl Pts',(-26.4858349192569,22.2203898942174,3.64849350137904));
#43040=CARTESIAN_POINT('Ctrl Pts',(-26.5084050487386,22.2705349643943,3.64509520766727));
#43041=CARTESIAN_POINT('Ctrl Pts',(-26.5268209493351,22.3139744724767,3.64214730061621));
#43042=CARTESIAN_POINT('Ctrl Pts',(-26.5815694784785,22.4514377936207,3.63279965841365));
#43043=CARTESIAN_POINT('Ctrl Pts',(-26.614446234285,22.5467637500771,3.62628775400308));
#43044=CARTESIAN_POINT('Ctrl Pts',(-26.729272943672,22.9383740710023,3.59943465296249));
#43045=CARTESIAN_POINT('Ctrl Pts',(-26.7731038549109,23.2440755629043,3.57805985896633));
#43046=CARTESIAN_POINT('Ctrl Pts',(-26.7730023558368,23.5513171860199,3.55804726516272));
#43047=CARTESIAN_POINT('Ctrl Pts',(-26.7730023545155,23.5513211782174,3.55804700512569));
#43048=CARTESIAN_POINT('Ctrl Pts',(-26.7729832548478,23.6089206270496,3.5542951907194));
#43049=CARTESIAN_POINT('Ctrl Pts',(-26.7714199600787,23.6665144938145,3.55060172167451));
#43050=CARTESIAN_POINT('Ctrl Pts',(-26.7680777749399,23.7284023229884,3.54671699804464));
#43051=CARTESIAN_POINT('Ctrl Pts',(-26.7678333450828,23.7327637753233,3.54644367868682));
#43052=CARTESIAN_POINT('Ctrl Pts',(-26.7674266535249,23.739765671965,3.54600562888445));
#43053=CARTESIAN_POINT('Ctrl Pts',(-26.7672700082726,23.7424064179969,3.54584058828782));
#43054=CARTESIAN_POINT('Ctrl Pts',(-26.7669933752814,23.7469747665552,3.54555537229685));
#43055=CARTESIAN_POINT('Ctrl Pts',(-26.7668749062878,23.748902454426,3.54543511184088));
#43056=CARTESIAN_POINT('Ctrl Pts',(-26.7666457701686,23.7525769283429,3.54520605163458));
#43057=CARTESIAN_POINT('Ctrl Pts',(-26.7665354127903,23.7543237319809,3.54509723438252));
#43058=CARTESIAN_POINT('Ctrl Pts',(-26.7663018245475,23.7579738503119,3.54487000881177));
#43059=CARTESIAN_POINT('Ctrl Pts',(-26.7661783270661,23.7598771461006,3.54475161599882));
#43060=CARTESIAN_POINT('Ctrl Pts',(-26.7659023405037,23.7640728959666,3.54449082009936));
#43061=CARTESIAN_POINT('Ctrl Pts',(-26.7657490891901,23.7663653029111,3.54434846023585));
#43062=CARTESIAN_POINT('Ctrl Pts',(-26.7652053520294,23.774370156927,3.54385180061354));
#43063=CARTESIAN_POINT('Ctrl Pts',(-26.7648020910703,23.7800817692397,3.54349821919257));
#43064=CARTESIAN_POINT('Ctrl Pts',(-26.7605787522617,23.8377126439053,3.53993828545128));
#43065=CARTESIAN_POINT('Ctrl Pts',(-26.7555161226822,23.8895368274097,3.53680048888148));
#43066=CARTESIAN_POINT('Ctrl Pts',(-26.7477668696566,23.952942372934,3.53301462335436));
#43067=CARTESIAN_POINT('Ctrl Pts',(-26.7462696357952,23.9646578010469,3.53231734591374));
#43068=CARTESIAN_POINT('Ctrl Pts',(-26.7006301938124,24.3068050412611,3.51201202278428));
#43069=CARTESIAN_POINT('Ctrl Pts',(-26.6055491089283,24.6284312303505,3.49431771996669));
#43070=CARTESIAN_POINT('Ctrl Pts',(-26.4295177855175,25.000079690047,3.47051216199984));
#43071=CARTESIAN_POINT('Ctrl Pts',(-26.3936918313434,25.0691398716863,3.46594238409155));
#43072=CARTESIAN_POINT('Ctrl Pts',(-26.3359506809717,25.1712290720934,3.45892010181078));
#43073=CARTESIAN_POINT('Ctrl Pts',(-26.3158661236785,25.2052632177996,3.45653259031974));
#43074=CARTESIAN_POINT('Ctrl Pts',(-26.2912621408161,25.2452567398001,3.45366817223913));
#43075=CARTESIAN_POINT('Ctrl Pts',(-26.287340851671,25.2515815621807,3.45321340121067));
#43076=CARTESIAN_POINT('Ctrl Pts',(-26.2812678845662,25.2613015846225,3.45251174615104));
#43077=CARTESIAN_POINT('Ctrl Pts',(-26.2791316843896,25.2647064648459,3.45226543551542));
#43078=CARTESIAN_POINT('Ctrl Pts',(-26.2753816631374,25.2706588423165,3.45183391577181));
#43079=CARTESIAN_POINT('Ctrl Pts',(-26.2737706225249,25.2732080927841,3.45164881009189));
#43080=CARTESIAN_POINT('Ctrl Pts',(-26.2701216319553,25.2789642130425,3.45123017437348));
#43081=CARTESIAN_POINT('Ctrl Pts',(-26.2680815866563,25.2821697432236,3.45099656652647));
#43082=CARTESIAN_POINT('Ctrl Pts',(-26.2625677964255,25.2907998479718,3.45036635249445));
#43083=CARTESIAN_POINT('Ctrl Pts',(-26.2590834623374,25.2962176068667,3.44996935151409));
#43084=CARTESIAN_POINT('Ctrl Pts',(-26.2436273929557,25.3200924699334,3.44821376696568));
#43085=CARTESIAN_POINT('Ctrl Pts',(-26.2314833165106,25.3384368035601,3.44684873394499));
#43086=CARTESIAN_POINT('Ctrl Pts',(-26.2104784106609,25.3694708592442,3.44451134506712));
#43087=CARTESIAN_POINT('Ctrl Pts',(-26.2017121315148,25.3822238817568,3.44354261114887));
#43088=CARTESIAN_POINT('Ctrl Pts',(-26.1864387056822,25.4041041048179,3.44186621106304));
#43089=CARTESIAN_POINT('Ctrl Pts',(-26.1799751085338,25.4132614857394,3.44116020993179));
#43090=CARTESIAN_POINT('Ctrl Pts',(-26.1726465211284,25.4235302224492,3.44036354701902));
#43091=CARTESIAN_POINT('Ctrl Pts',(-26.1718283570184,25.4246750386459,3.44027466059285));
#43092=CARTESIAN_POINT('Ctrl Pts',(-26.1639336096302,25.4357064846877,3.43941747583576));
#43093=CARTESIAN_POINT('Ctrl Pts',(-26.156801959169,25.4455534211798,3.4386470986145));
#43094=CARTESIAN_POINT('Ctrl Pts',(-26.1472639788668,25.4585672124211,3.43762196478568));
#43095=CARTESIAN_POINT('Ctrl Pts',(-26.1449071945639,25.4617703991617,3.43736907415336));
#43096=CARTESIAN_POINT('Ctrl Pts',(-26.1392629926044,25.4694119576199,3.43676441944088));
#43097=CARTESIAN_POINT('Ctrl Pts',(-26.1359700899193,25.473846245894,3.43641245043136));
#43098=CARTESIAN_POINT('Ctrl Pts',(-26.1238802525535,25.4900395244221,3.43512309561724));
#43099=CARTESIAN_POINT('Ctrl Pts',(-26.1150144700019,25.5017466801418,3.4341831497172));
#43100=CARTESIAN_POINT('Ctrl Pts',(-25.9477497217723,25.719509030779,3.41655287160166));
#43101=CARTESIAN_POINT('Ctrl Pts',(-25.765097918075,25.9056895297535,3.39889550684495));
#43102=CARTESIAN_POINT('Ctrl Pts',(-25.4968350405726,26.1200616863566,3.3757115820829));
#43103=CARTESIAN_POINT('Ctrl Pts',(-25.4295365377656,26.1696790947764,3.37009991888696));
#43104=CARTESIAN_POINT('Ctrl Pts',(-25.3102755607003,26.2506421845818,3.36058552815684));
#43105=CARTESIAN_POINT('Ctrl Pts',(-25.2592163476026,26.2832415611422,3.35663984614454));
#43106=CARTESIAN_POINT('Ctrl Pts',(-25.1916005642599,26.3237751593491,3.3516073101922));
#43107=CARTESIAN_POINT('Ctrl Pts',(-25.1758558258971,26.3330326335966,3.35044869122838));
#43108=CARTESIAN_POINT('Ctrl Pts',(-25.1535567872937,26.3458900096894,3.34882724061706));
#43109=CARTESIAN_POINT('Ctrl Pts',(-25.1470677020797,26.3496015200517,3.34835769839622));
#43110=CARTESIAN_POINT('Ctrl Pts',(-25.135722519459,26.3560382482091,3.347540867666));
#43111=CARTESIAN_POINT('Ctrl Pts',(-25.130872195773,26.3587735032618,3.34719295276691));
#43112=CARTESIAN_POINT('Ctrl Pts',(-25.1238216135272,26.3627255054854,3.34668912275339));
#43113=CARTESIAN_POINT('Ctrl Pts',(-25.1216270161875,26.3639522514927,3.34653256611084));
#43114=CARTESIAN_POINT('Ctrl Pts',(-25.1178825228433,26.3660396181315,3.34626590347966));
#43115=CARTESIAN_POINT('Ctrl Pts',(-25.1163333508096,26.366901528881,3.34615571368073));
#43116=CARTESIAN_POINT('Ctrl Pts',(-25.113250046242,26.368613652702,3.34593667115952));
#43117=CARTESIAN_POINT('Ctrl Pts',(-25.1117159325408,26.3694638906995,3.34582781681194));
#43118=CARTESIAN_POINT('Ctrl Pts',(-25.1081001702286,26.3714639652756,3.34557156480758));
#43119=CARTESIAN_POINT('Ctrl Pts',(-25.1060179380628,26.372612752908,3.34542423516249));
#43120=CARTESIAN_POINT('Ctrl Pts',(-25.099863628826,26.3759992647313,3.34498948543377));
#43121=CARTESIAN_POINT('Ctrl Pts',(-25.0957879595578,26.378230500753,3.3447024810362));
#43122=CARTESIAN_POINT('Ctrl Pts',(-25.0602458323582,26.3975883479053,3.34220740698612));
#43123=CARTESIAN_POINT('Ctrl Pts',(-25.0284990660371,26.4141988412201,3.34003170514781));
#43124=CARTESIAN_POINT('Ctrl Pts',(-24.8466973350538,26.5054920537614,3.32783265651303));
#43125=CARTESIAN_POINT('Ctrl Pts',(-24.6912554534103,26.5689171250461,3.31838960395227));
#43126=CARTESIAN_POINT('Ctrl Pts',(-24.5151280379785,26.6252209397543,3.30804020957837));
#43127=CARTESIAN_POINT('Ctrl Pts',(-24.4986461325155,26.6303442565683,3.30707509553081));
#43128=CARTESIAN_POINT('Ctrl Pts',(-24.4633785338458,26.6409970881002,3.3050158436721));
#43129=CARTESIAN_POINT('Ctrl Pts',(-24.4445820072437,26.646488278328,3.30392186136501));
#43130=CARTESIAN_POINT('Ctrl Pts',(-24.4040347995071,26.6579336439278,3.30156767792024));
#43131=CARTESIAN_POINT('Ctrl Pts',(-24.3822693445967,26.663831513458,3.30030748184477));
#43132=CARTESIAN_POINT('Ctrl Pts',(-24.334803316005,26.6761603068449,3.29756410622653));
#43133=CARTESIAN_POINT('Ctrl Pts',(-24.3090817950271,26.6825037168355,3.29608055927804));
#43134=CARTESIAN_POINT('Ctrl Pts',(-24.2520327919579,26.6958291124097,3.2927925860077));
#43135=CARTESIAN_POINT('Ctrl Pts',(-24.220673487355,26.7026616515778,3.29098683570275));
#43136=CARTESIAN_POINT('Ctrl Pts',(-24.1489242629813,26.7171752832638,3.28685166525733));
#43137=CARTESIAN_POINT('Ctrl Pts',(-24.1084793644934,26.7245540661802,3.28451802296216));
#43138=CARTESIAN_POINT('Ctrl Pts',(-23.9654117324493,26.7478365426071,3.27623235892892));
#43139=CARTESIAN_POINT('Ctrl Pts',(-23.8621804969453,26.7595513054382,3.27019585559012));
#43140=CARTESIAN_POINT('Ctrl Pts',(-23.71086418142,26.7693528539763,3.26115476456382));
#43141=CARTESIAN_POINT('Ctrl Pts',(-23.6630972792925,26.7713810106407,3.25827330576143));
#43142=CARTESIAN_POINT('Ctrl Pts',(-23.6074673147068,26.77250414854,3.25488013295656));
#43143=CARTESIAN_POINT('Ctrl Pts',(-23.5996293367874,26.7726337852189,3.25440119245355));
#43144=CARTESIAN_POINT('Ctrl Pts',(-23.5876871381631,26.772787722715,3.25367012772748));
#43145=CARTESIAN_POINT('Ctrl Pts',(-23.5835831760688,26.7728327828326,3.25341865554086));
#43146=CARTESIAN_POINT('Ctrl Pts',(-23.5761337030236,26.7729003437323,3.25296174544063));
#43147=CARTESIAN_POINT('Ctrl Pts',(-23.5727882168216,26.7729254747997,3.25275639040534));
#43148=CARTESIAN_POINT('Ctrl Pts',(-23.5660911285918,26.7729653539649,3.252344979996));
#43149=CARTESIAN_POINT('Ctrl Pts',(-23.5627395306083,26.7729800831176,3.25213892428086));
#43150=CARTESIAN_POINT('Ctrl Pts',(-23.5532843201772,26.7730068855131,3.25155715660602));
#43151=CARTESIAN_POINT('Ctrl Pts',(-23.5471807116872,26.7730068474778,3.25118106483601));
#43152=CARTESIAN_POINT('Ctrl Pts',(-23.521903414878,26.7729348812405,3.24962124909498));
#43153=CARTESIAN_POINT('Ctrl Pts',(-23.5027308682403,26.7727091822049,3.24843270808397));
#43154=CARTESIAN_POINT('Ctrl Pts',(-23.0905919617589,26.7641786631398,3.22276273278232));
#43155=CARTESIAN_POINT('Ctrl Pts',(-22.7024758212538,26.6842111484528,3.19562396212885));
#43156=CARTESIAN_POINT('Ctrl Pts',(-22.2763646369559,26.5113032920142,3.16504511848092));
#43157=CARTESIAN_POINT('Ctrl Pts',(-22.2150410859821,26.4841618004785,3.16064001582726));
#43158=CARTESIAN_POINT('Ctrl Pts',(-22.1306381683155,26.4436103775033,3.15461247963233));
#43159=CARTESIAN_POINT('Ctrl Pts',(-22.1068138473911,26.4317988932988,3.15291518387263));
#43160=CARTESIAN_POINT('Ctrl Pts',(-22.0804351126803,26.4183117238683,3.15104271709831));
#43161=CARTESIAN_POINT('Ctrl Pts',(-22.0777345880461,26.4169261581847,3.15085110340496));
#43162=CARTESIAN_POINT('Ctrl Pts',(-22.0750360153455,26.415536774556,3.15065971150053));
#43163=CARTESIAN_POINT('Ctrl Pts',(-22.0750360171757,26.4155367754983,2.90599376073417));
#43164=CARTESIAN_POINT('Ctrl Pts',(-22.0989936332936,26.4278715625345,2.90780143374778));
#43165=CARTESIAN_POINT('Ctrl Pts',(-22.1231118065676,26.439908887829,2.90961461478517));
#43166=CARTESIAN_POINT('Ctrl Pts',(-22.2949730071992,26.5230063774932,2.92248205540678));
#43167=CARTESIAN_POINT('Ctrl Pts',(-22.4477913926813,26.5830026121293,2.93366489442656));
#43168=CARTESIAN_POINT('Ctrl Pts',(-22.6753219197806,26.652848285626,2.94948805524692));
#43169=CARTESIAN_POINT('Ctrl Pts',(-22.7468652453027,26.6721389103886,2.95434734426875));
#43170=CARTESIAN_POINT('Ctrl Pts',(-22.8504845629538,26.6962796198166,2.96116208954661));
#43171=CARTESIAN_POINT('Ctrl Pts',(-22.8820641421926,26.7031378965749,2.96320960364302));
#43172=CARTESIAN_POINT('Ctrl Pts',(-22.9182408451525,26.7104265526037,2.96551758846153));
#43173=CARTESIAN_POINT('Ctrl Pts',(-22.9227406591764,26.7113231517259,2.96580400383328));
#43174=CARTESIAN_POINT('Ctrl Pts',(-22.9295295812564,26.7126607936927,2.96623510859841));
#43175=CARTESIAN_POINT('Ctrl Pts',(-22.9318172537725,26.7131089628117,2.96638020517512));
#43176=CARTESIAN_POINT('Ctrl Pts',(-22.9359216704411,26.7139084199559,2.96664021603863));
#43177=CARTESIAN_POINT('Ctrl Pts',(-22.9377382269104,26.7142606247488,2.96675518292943));
#43178=CARTESIAN_POINT('Ctrl Pts',(-22.9416533984469,26.7150162234024,2.96700272986064));
#43179=CARTESIAN_POINT('Ctrl Pts',(-22.9437521061084,26.7154190933734,2.96713527922917));
#43180=CARTESIAN_POINT('Ctrl Pts',(-22.9493809484864,26.7164938074274,2.96749039341344));
#43181=CARTESIAN_POINT('Ctrl Pts',(-22.9529118218381,26.7171618376755,2.96771273903431));
#43182=CARTESIAN_POINT('Ctrl Pts',(-22.9689218135657,26.720163150408,2.9687190846058));
#43183=CARTESIAN_POINT('Ctrl Pts',(-22.9814137588918,26.7224286298396,2.96949924911447));
#43184=CARTESIAN_POINT('Ctrl Pts',(-22.9963169188284,26.7250405286924,2.97042434608434));
#43185=CARTESIAN_POINT('Ctrl Pts',(-22.9987153128324,26.7254580660489,2.97057304938576));
#43186=CARTESIAN_POINT('Ctrl Pts',(-23.338424615989,26.7842016761861,2.99161104615214));
#43187=CARTESIAN_POINT('Ctrl Pts',(-23.6829383325917,26.7884295990645,3.00972498877603));
#43188=CARTESIAN_POINT('Ctrl Pts',(-24.1611171660068,26.7177152813727,3.03728306588256));
#43189=CARTESIAN_POINT('Ctrl Pts',(-24.2990017231632,26.6879814838444,3.04549513567131));
#43190=CARTESIAN_POINT('Ctrl Pts',(-24.4483976968447,26.6453554493543,3.0548841515702));
#43191=CARTESIAN_POINT('Ctrl Pts',(-24.462280848853,26.6412929951535,3.05576133633806));
#43192=CARTESIAN_POINT('Ctrl Pts',(-24.4831947751676,26.6350200499408,3.05709000413791));
#43193=CARTESIAN_POINT('Ctrl Pts',(-24.4902462127574,26.6328786441885,3.05753923379858));
#43194=CARTESIAN_POINT('Ctrl Pts',(-24.5016471225592,26.6293736192669,3.05826760596024));
#43195=CARTESIAN_POINT('Ctrl Pts',(-24.5060011828787,26.6280249168593,3.0585462593459));
#43196=CARTESIAN_POINT('Ctrl Pts',(-24.5143424234533,26.6254217488942,3.0590810223188));
#43197=CARTESIAN_POINT('Ctrl Pts',(-24.5183300558334,26.6241687538451,3.0593370831641));
#43198=CARTESIAN_POINT('Ctrl Pts',(-24.5254593581988,26.6219133337678,3.05979562217393));
#43199=CARTESIAN_POINT('Ctrl Pts',(-24.5286019540289,26.6209138358994,3.05999800367246));
#43200=CARTESIAN_POINT('Ctrl Pts',(-24.5348439661779,26.6189180183025,3.06040050024886));
#43201=CARTESIAN_POINT('Ctrl Pts',(-24.5379434182411,26.6179218218997,3.0606006110653));
#43202=CARTESIAN_POINT('Ctrl Pts',(-24.5463935144951,26.6151917383836,3.06114686867473));
#43203=CARTESIAN_POINT('Ctrl Pts',(-24.5517411189934,26.6134485435721,3.06149332248889));
#43204=CARTESIAN_POINT('Ctrl Pts',(-24.5719781460097,26.6067930855152,3.06280730348278));
#43205=CARTESIAN_POINT('Ctrl Pts',(-24.5868360258536,26.6017862499679,3.06377795489912));
#43206=CARTESIAN_POINT('Ctrl Pts',(-24.8327463854409,26.5169157288822,3.07994343978659));
#43207=CARTESIAN_POINT('Ctrl Pts',(-25.0539605128634,26.4111432347182,3.09605415401928));
#43208=CARTESIAN_POINT('Ctrl Pts',(-25.3230185329993,26.2426054918427,3.11748583416924));
#43209=CARTESIAN_POINT('Ctrl Pts',(-25.3836440650742,26.201693485333,3.12244243948128));
#43210=CARTESIAN_POINT('Ctrl Pts',(-25.5016262062503,26.1160927465489,3.13229857733408));
#43211=CARTESIAN_POINT('Ctrl Pts',(-25.5589698419306,26.0714527717369,3.13719555983923));
#43212=CARTESIAN_POINT('Ctrl Pts',(-25.6690725541822,25.9795986749205,3.14675104227998));
#43213=CARTESIAN_POINT('Ctrl Pts',(-25.721885176897,25.9325065096503,3.15140991264535));
#43214=CARTESIAN_POINT('Ctrl Pts',(-25.7937009824346,25.8640946772698,3.15780528426843));
#43215=CARTESIAN_POINT('Ctrl Pts',(-25.8140338233024,25.8442056298425,3.15962306742239));
#43216=CARTESIAN_POINT('Ctrl Pts',(-25.8452067335706,25.8128949073135,3.16241734265421));
#43217=CARTESIAN_POINT('Ctrl Pts',(-25.856230393439,25.8016590773704,3.16340695235446));
#43218=CARTESIAN_POINT('Ctrl Pts',(-25.8697715878855,25.7876534574243,3.16462387567916));
#43219=CARTESIAN_POINT('Ctrl Pts',(-25.8723669515102,25.7849597107478,3.16485717668209));
#43220=CARTESIAN_POINT('Ctrl Pts',(-25.876446058391,25.7807111969685,3.16522393951557));
#43221=CARTESIAN_POINT('Ctrl Pts',(-25.8779329360597,25.7791594647762,3.16535764651394));
#43222=CARTESIAN_POINT('Ctrl Pts',(-25.8807085101094,25.7762570196272,3.16560727086978));
#43223=CARTESIAN_POINT('Ctrl Pts',(-25.881997576392,25.7749066832835,3.16572321708077));
#43224=CARTESIAN_POINT('Ctrl Pts',(-25.8848880389779,25.7718735630103,3.1659832314401));
#43225=CARTESIAN_POINT('Ctrl Pts',(-25.8864887861347,25.7701901709505,3.16612724855639));
#43226=CARTESIAN_POINT('Ctrl Pts',(-25.8905510674399,25.7659088981338,3.16649278303106));
#43227=CARTESIAN_POINT('Ctrl Pts',(-25.8930101042013,25.7633086374679,3.16671410617596));
#43228=CARTESIAN_POINT('Ctrl Pts',(-25.9065191505064,25.7489760099786,3.16793030137597));
#43229=CARTESIAN_POINT('Ctrl Pts',(-25.9174856201728,25.737164702583,3.16891880007298));
#43230=CARTESIAN_POINT('Ctrl Pts',(-26.1448225195932,25.4886002648009,3.18944860111491));
#43231=CARTESIAN_POINT('Ctrl Pts',(-26.3247809329327,25.2208988454348,3.20656226704444));
#43232=CARTESIAN_POINT('Ctrl Pts',(-26.4965209262014,24.858694404708,3.22928268032653));
#43233=CARTESIAN_POINT('Ctrl Pts',(-26.5280903869415,24.7851606868751,3.23386565412394));
#43234=CARTESIAN_POINT('Ctrl Pts',(-26.5768317653921,24.6588569144059,3.24175600984534));
#43235=CARTESIAN_POINT('Ctrl Pts',(-26.5954370196622,24.6066787969809,3.24502057228894));
#43236=CARTESIAN_POINT('Ctrl Pts',(-26.6265686624351,24.5117007622894,3.25098964371017));
#43237=CARTESIAN_POINT('Ctrl Pts',(-26.6395690664385,24.4690706214227,3.25367825951521));
#43238=CARTESIAN_POINT('Ctrl Pts',(-26.6537723117052,24.4187810274552,3.25686540466728));
#43239=CARTESIAN_POINT('Ctrl Pts',(-26.6558371997508,24.4113684593025,3.25733557016836));
#43240=CARTESIAN_POINT('Ctrl Pts',(-26.6589546461619,24.4000203364137,3.25805597734139));
#43241=CARTESIAN_POINT('Ctrl Pts',(-26.6600263320696,24.3960900271323,3.2583055960804));
#43242=CARTESIAN_POINT('Ctrl Pts',(-26.661879781196,24.3892415361533,3.25874075248496));
#43243=CARTESIAN_POINT('Ctrl Pts',(-26.6626649003459,24.3863242611589,3.25892618078188));
#43244=CARTESIAN_POINT('Ctrl Pts',(-26.664295489136,24.3802313394254,3.25931359385866));
#43245=CARTESIAN_POINT('Ctrl Pts',(-26.6651402053918,24.3770554962492,3.25951560287189));
#43246=CARTESIAN_POINT('Ctrl Pts',(-26.6674567397874,24.3682921845604,3.26007323159049));
#43247=CARTESIAN_POINT('Ctrl Pts',(-26.6689183857874,24.36270206147,3.26042918095005));
#43248=CARTESIAN_POINT('Ctrl Pts',(-26.6745557747331,24.3409022637657,3.26181822358134));
#43249=CARTESIAN_POINT('Ctrl Pts',(-26.678620178932,24.3246643084591,3.26285491637539));
#43250=CARTESIAN_POINT('Ctrl Pts',(-26.7428889505068,24.0591347478432,3.27984254051787));
#43251=CARTESIAN_POINT('Ctrl Pts',(-26.7732386265911,23.8036188887567,3.29680855311751));
#43252=CARTESIAN_POINT('Ctrl Pts',(-26.7727849374212,23.3138716996363,3.32991413507576));
#43253=CARTESIAN_POINT('Ctrl Pts',(-26.7472155478491,23.0811683706983,3.345863258448));
#43254=CARTESIAN_POINT('Ctrl Pts',(-26.6936828479454,22.8395052829816,3.36149878070361));
#43255=CARTESIAN_POINT('Ctrl Pts',(-26.6905476061964,22.8257784693161,3.36238346584647));
#43256=CARTESIAN_POINT('Ctrl Pts',(-26.6864664269478,22.8084345404668,3.36349653431896));
#43257=CARTESIAN_POINT('Ctrl Pts',(-26.6856040866437,22.8047982030439,3.36372963668976));
#43258=CARTESIAN_POINT('Ctrl Pts',(-26.6842309005448,22.7990522539057,3.36409754598886));
#43259=CARTESIAN_POINT('Ctrl Pts',(-26.683724248863,22.7969416585863,3.36423259488973));
#43260=CARTESIAN_POINT('Ctrl Pts',(-26.6827782930441,22.7930184890381,3.36448345193259));
#43261=CARTESIAN_POINT('Ctrl Pts',(-26.6823395505057,22.7912057956487,3.36459929161221));
#43262=CARTESIAN_POINT('Ctrl Pts',(-26.681357431404,22.7871634569367,3.36485746433009));
#43263=CARTESIAN_POINT('Ctrl Pts',(-26.6808132479863,22.7849340158538,3.3649997495779));
#43264=CARTESIAN_POINT('Ctrl Pts',(-26.679215391581,22.7784180491853,3.36541530971551));
#43265=CARTESIAN_POINT('Ctrl Pts',(-26.6781552873184,22.7741330828651,3.36568821209387));
#43266=CARTESIAN_POINT('Ctrl Pts',(-26.6703930846981,22.7430323040894,3.36766634000781));
#43267=CARTESIAN_POINT('Ctrl Pts',(-26.6633547838917,22.7163004601444,3.36935238514386));
#43268=CARTESIAN_POINT('Ctrl Pts',(-26.6397348684566,22.6310603779597,3.37469282748858));
#43269=CARTESIAN_POINT('Ctrl Pts',(-26.6218401306455,22.5729266118457,3.37828064645739));
#43270=CARTESIAN_POINT('Ctrl Pts',(-26.5754546339251,22.4361325727833,3.38666882186064));
#43271=CARTESIAN_POINT('Ctrl Pts',(-26.5455255254633,22.3580058285708,3.39141631390109));
#43272=CARTESIAN_POINT('Ctrl Pts',(-26.4102190307824,22.0421790549289,3.41075047897424));
#43273=CARTESIAN_POINT('Ctrl Pts',(-26.2793234251647,21.8165107777194,3.42499384675426));
#43274=CARTESIAN_POINT('Ctrl Pts',(-26.1144895840033,21.5980758638406,3.44105155145121));
#43275=CARTESIAN_POINT('Ctrl Pts',(-26.106164409712,21.5871886338585,3.44185814348597));
#43276=CARTESIAN_POINT('Ctrl Pts',(-26.090901814393,21.5674906867641,3.44332917448825));
#43277=CARTESIAN_POINT('Ctrl Pts',(-26.0839873437853,21.5586624109682,3.44399278938118));
#43278=CARTESIAN_POINT('Ctrl Pts',(-26.0739568549818,21.5459924397679,3.44495155256351));
#43279=CARTESIAN_POINT('Ctrl Pts',(-26.0708777999388,21.5421214891154,3.44524533911121));
#43280=CARTESIAN_POINT('Ctrl Pts',(-26.0634600459117,21.5328399184325,3.44595185960675));
#43281=CARTESIAN_POINT('Ctrl Pts',(-26.0591127814491,21.5274362009849,3.44636491180175));
#43282=CARTESIAN_POINT('Ctrl Pts',(-26.0535114783011,21.5205195270943,3.44689584336933));
#43283=CARTESIAN_POINT('Ctrl Pts',(-26.0522734297748,21.5189935995851,3.44701311519233));
#43284=CARTESIAN_POINT('Ctrl Pts',(-26.0475829044676,21.5132231978584,3.44745711819831));
#43285=CARTESIAN_POINT('Ctrl Pts',(-26.0441210301028,21.5089864025998,3.44778420746588));
#43286=CARTESIAN_POINT('Ctrl Pts',(-26.0388206087923,21.5025331219345,3.44828409255519));
#43287=CARTESIAN_POINT('Ctrl Pts',(-26.0369898410376,21.500310237458,3.44845658730477));
#43288=CARTESIAN_POINT('Ctrl Pts',(-26.0226246224643,21.4829158161413,3.44980878919475));
#43289=CARTESIAN_POINT('Ctrl Pts',(-26.0099546338039,21.4678571817102,3.45099375932787));
#43290=CARTESIAN_POINT('Ctrl Pts',(-25.984304473937,21.4379319668035,3.4533782163696));
#43291=CARTESIAN_POINT('Ctrl Pts',(-25.9713240850451,21.4230667069491,3.45457768286575));
#43292=CARTESIAN_POINT('Ctrl Pts',(-25.9541047369771,21.4037087382997,3.4561598893506));
#43293=CARTESIAN_POINT('Ctrl Pts',(-25.9499880415281,21.3991074496954,3.45653749162365));
#43294=CARTESIAN_POINT('Ctrl Pts',(-25.9436066407195,21.3920159827923,3.45712181611206));
#43295=CARTESIAN_POINT('Ctrl Pts',(-25.9413511980089,21.3895174576939,3.45732814670621));
#43296=CARTESIAN_POINT('Ctrl Pts',(-25.9368469877599,21.3845434908558,3.4577398154555));
#43297=CARTESIAN_POINT('Ctrl Pts',(-25.9345982728858,21.3820680068852,3.45794515124021));
#43298=CARTESIAN_POINT('Ctrl Pts',(-25.9295975943158,21.3765802282549,3.45840136008007));
#43299=CARTESIAN_POINT('Ctrl Pts',(-25.9268437586165,21.3735696540953,3.45865231263446));
#43300=CARTESIAN_POINT('Ctrl Pts',(-25.9188598286573,21.3648746004018,3.45937907795272));
#43301=CARTESIAN_POINT('Ctrl Pts',(-25.9136150316124,21.3592037138624,3.45985551856304));
#43302=CARTESIAN_POINT('Ctrl Pts',(-25.8775357133785,21.320473565285,3.46312634969951));
#43303=CARTESIAN_POINT('Ctrl Pts',(-25.8460302493492,21.288048831281,3.46594959421429));
#43304=CARTESIAN_POINT('Ctrl Pts',(-25.7571780974443,21.200372303213,3.47382793989629));
#43305=CARTESIAN_POINT('Ctrl Pts',(-25.698452900415,21.1465697393773,3.47894351358443));
#43306=CARTESIAN_POINT('Ctrl Pts',(-25.4101861273518,20.9014745697645,3.50363535933499));
#43307=CARTESIAN_POINT('Ctrl Pts',(-25.1568140257935,20.740573695822,3.52431361361684));
#43308=CARTESIAN_POINT('Ctrl Pts',(-24.8037581919339,20.5799333364377,3.54996096298823));
#43309=CARTESIAN_POINT('Ctrl Pts',(-24.7210681482117,20.5463772350149,3.55575003065747));
#43310=CARTESIAN_POINT('Ctrl Pts',(-24.631058342462,20.5141337379637,3.56174377971457));
#43311=CARTESIAN_POINT('Ctrl Pts',(-24.6250262094685,20.5119931495046,3.56214399984));
#43312=CARTESIAN_POINT('Ctrl Pts',(-24.6166520601033,20.5090495234321,3.56269754664557));
#43313=CARTESIAN_POINT('Ctrl Pts',(-24.6143154873417,20.5082312105701,3.56285177628456));
#43314=CARTESIAN_POINT('Ctrl Pts',(-24.6102978352894,20.5068293466376,3.56311658400636));
#43315=CARTESIAN_POINT('Ctrl Pts',(-24.6086172160655,20.5062444955804,3.56322723986907));
#43316=CARTESIAN_POINT('Ctrl Pts',(-24.6051806019271,20.5050517530652,3.56345327711326));
#43317=CARTESIAN_POINT('Ctrl Pts',(-24.6034245691066,20.5044439895902,3.56356865028646));
#43318=CARTESIAN_POINT('Ctrl Pts',(-24.5993235463136,20.5030285950582,3.5638377976133));
#43319=CARTESIAN_POINT('Ctrl Pts',(-24.5969781420184,20.5022221495437,3.56399150063066));
#43320=CARTESIAN_POINT('Ctrl Pts',(-24.592024761747,20.5005253672808,3.56431564532827));
#43321=CARTESIAN_POINT('Ctrl Pts',(-24.5894165679321,20.4996356657809,3.5644860492163));
#43322=CARTESIAN_POINT('Ctrl Pts',(-24.5824183056959,20.4972584500192,3.56494254777384));
#43323=CARTESIAN_POINT('Ctrl Pts',(-24.5780261434918,20.4957770527809,3.56522828388908));
#43324=CARTESIAN_POINT('Ctrl Pts',(-24.4733063868518,20.4607084126243,3.57202303196094));
#43325=CARTESIAN_POINT('Ctrl Pts',(-24.3713759377099,20.4320682803523,3.57824640516057));
#43326=CARTESIAN_POINT('Ctrl Pts',(-23.8874125799282,20.3214726556528,3.60677963174904));
#43327=CARTESIAN_POINT('Ctrl Pts',(-23.4939872160089,20.3043982820673,3.62751379813933));
#43328=CARTESIAN_POINT('Ctrl Pts',(-23.0878489475399,20.3607892981768,3.65232537993949));
#43329=CARTESIAN_POINT('Ctrl Pts',(-23.0686868977944,20.3636262110622,3.65350287765477));
#43330=CARTESIAN_POINT('Ctrl Pts',(-23.0434975922354,20.3675878375705,3.6550601533472));
#43331=CARTESIAN_POINT('Ctrl Pts',(-23.0374460393098,20.3685572878916,3.65543499385223));
#43332=CARTESIAN_POINT('Ctrl Pts',(-23.0280842915022,20.3700844292698,3.65601599264663));
#43333=CARTESIAN_POINT('Ctrl Pts',(-23.0247721180224,20.3706300438108,3.65622176656641));
#43334=CARTESIAN_POINT('Ctrl Pts',(-23.018490897518,20.3716748322579,3.65661241186834));
#43335=CARTESIAN_POINT('Ctrl Pts',(-23.0155216837761,20.3721729941241,3.65679725084986));
#43336=CARTESIAN_POINT('Ctrl Pts',(-23.008657000496,20.3733346136517,3.65722499883446));
#43337=CARTESIAN_POINT('Ctrl Pts',(-23.0047620503207,20.3740010756688,3.65746800329421));
#43338=CARTESIAN_POINT('Ctrl Pts',(-22.993844864898,20.3758897804332,3.65814998215052));
#43339=CARTESIAN_POINT('Ctrl Pts',(-22.9868254764664,20.3771281533579,3.65858947010189));
#43340=CARTESIAN_POINT('Ctrl Pts',(-22.9462081383265,20.384432960337,3.66113838770059));
#43341=CARTESIAN_POINT('Ctrl Pts',(-22.91270522459,20.3910095093719,3.66326404451808));
#43342=CARTESIAN_POINT('Ctrl Pts',(-22.816316937916,20.4115259499161,3.66944929255788));
#43343=CARTESIAN_POINT('Ctrl Pts',(-22.7537398199039,20.4268197149286,3.67355144717675));
#43344=CARTESIAN_POINT('Ctrl Pts',(-22.6152221601491,20.4651065181626,3.68283001773376));
#43345=CARTESIAN_POINT('Ctrl Pts',(-22.5395891295429,20.4890492258005,3.68803245350386));
#43346=CARTESIAN_POINT('Ctrl Pts',(-22.2032172980128,20.60935750785,3.711752463771));
#43347=CARTESIAN_POINT('Ctrl Pts',(-21.9547430153838,20.7364108178673,3.7310071596857));
#43348=CARTESIAN_POINT('Ctrl Pts',(-21.7222791946736,20.8960769848946,3.7493814562276));
#43349=CARTESIAN_POINT('Ctrl Pts',(-21.7189058500562,20.8984034247394,3.74964814709278));
#43350=CARTESIAN_POINT('Ctrl Pts',(-21.7097477079703,20.9047451809933,3.75037230906987));
#43351=CARTESIAN_POINT('Ctrl Pts',(-21.7039715858007,20.9087730562375,3.75082919126555));
#43352=CARTESIAN_POINT('Ctrl Pts',(-21.6971329620578,20.9135752380434,3.75137024776383));
#43353=CARTESIAN_POINT('Ctrl Pts',(-21.6960577209558,20.9143312707183,3.75145532230284));
#43354=CARTESIAN_POINT('Ctrl Pts',(-21.6863305929269,20.9211795886739,3.75222497897567));
#43355=CARTESIAN_POINT('Ctrl Pts',(-21.677708182226,20.9273138746077,3.75290746220585));
#43356=CARTESIAN_POINT('Ctrl Pts',(-21.6392266719494,20.9549774434047,3.75595387394875));
#43357=CARTESIAN_POINT('Ctrl Pts',(-21.6097060318157,20.976975983963,3.75829230266712));
#43358=CARTESIAN_POINT('Ctrl Pts',(-21.5765024389841,21.0026154874384,3.76091800778069));
#43359=CARTESIAN_POINT('Ctrl Pts',(-21.5724450702153,21.0057640597365,3.76123878267264));
#43360=CARTESIAN_POINT('Ctrl Pts',(-21.5664622907775,21.0104297325702,3.76171164353632));
#43361=CARTESIAN_POINT('Ctrl Pts',(-21.5645310822991,21.0119393326553,3.76186425932182));
#43362=CARTESIAN_POINT('Ctrl Pts',(-21.5611510260122,21.0145876960961,3.76213133197922));
#43363=CARTESIAN_POINT('Ctrl Pts',(-21.5597014315771,21.0157254996255,3.76224585769051));
#43364=CARTESIAN_POINT('Ctrl Pts',(-21.5566832311632,21.0180987067509,3.76248428365919));
#43365=CARTESIAN_POINT('Ctrl Pts',(-21.5551148001493,21.0193343225431,3.76260816800031));
#43366=CARTESIAN_POINT('Ctrl Pts',(-21.5519161416613,21.0218590587136,3.76286078834076));
#43367=CARTESIAN_POINT('Ctrl Pts',(-21.5502860104783,21.0231483003624,3.762989515532));
#43368=CARTESIAN_POINT('Ctrl Pts',(-21.5462970605318,21.026309366763,3.76330447734419));
#43369=CARTESIAN_POINT('Ctrl Pts',(-21.5439396100811,21.0281829269951,3.76349058814814));
#43370=CARTESIAN_POINT('Ctrl Pts',(-21.5374700555604,21.0333393522846,3.76400126022353));
#43371=CARTESIAN_POINT('Ctrl Pts',(-21.5333633374887,21.0366290061587,3.76432534243849));
#43372=CARTESIAN_POINT('Ctrl Pts',(-21.3851974835405,21.1559129780184,3.77601572596151));
#43373=CARTESIAN_POINT('Ctrl Pts',(-21.2513569883429,21.2841044578798,3.78651131054078));
#43374=CARTESIAN_POINT('Ctrl Pts',(-20.9243157965346,21.6563241458144,3.81429830373962));
#43375=CARTESIAN_POINT('Ctrl Pts',(-20.7541959166598,21.9179061362556,3.83138930546549));
#43376=CARTESIAN_POINT('Ctrl Pts',(-20.6162521152359,22.2167943651935,3.85131593533221));
#43377=CARTESIAN_POINT('Ctrl Pts',(-20.6085438388796,22.233886674851,3.85245595033117));
#43378=CARTESIAN_POINT('Ctrl Pts',(-20.598546474435,22.2565812012038,3.85397058952886));
#43379=CARTESIAN_POINT('Ctrl Pts',(-20.596123279732,22.2621242299689,3.85434060862077));
#43380=CARTESIAN_POINT('Ctrl Pts',(-20.5923861349425,22.2707389120592,3.85491580189394));
#43381=CARTESIAN_POINT('Ctrl Pts',(-20.5910613209305,22.2738058614927,3.85512060422722));
#43382=CARTESIAN_POINT('Ctrl Pts',(-20.5884187769462,22.2799495856547,3.85553091812981));
#43383=CARTESIAN_POINT('Ctrl Pts',(-20.5871010664563,22.2830263642695,3.8557364300579));
#43384=CARTESIAN_POINT('Ctrl Pts',(-20.5841704247533,22.2898988091019,3.85619553368689));
#43385=CARTESIAN_POINT('Ctrl Pts',(-20.5825599836731,22.2936955248956,3.85644920989676));
#43386=CARTESIAN_POINT('Ctrl Pts',(-20.5778730420384,22.3048045533091,3.85719158505529));
#43387=CARTESIAN_POINT('Ctrl Pts',(-20.5748162648527,22.3121251079005,3.85768095427069));
#43388=CARTESIAN_POINT('Ctrl Pts',(-20.5526661930566,22.3657272080596,3.86126548134028));
#43389=CARTESIAN_POINT('Ctrl Pts',(-20.534627554023,22.4124346033218,3.86439616792427));
#43390=CARTESIAN_POINT('Ctrl Pts',(-20.4794067766693,22.5659681108591,3.87471834383338));
#43391=CARTESIAN_POINT('Ctrl Pts',(-20.4467616862768,22.6743249018979,3.88205519070347));
#43392=CARTESIAN_POINT('Ctrl Pts',(-20.3394064415919,23.1129968649152,3.91192138687688));
#43393=CARTESIAN_POINT('Ctrl Pts',(-20.3112506221036,23.4524204255987,3.93564606072539));
#43394=CARTESIAN_POINT('Ctrl Pts',(-20.3367002153579,23.793587883721,3.95727599795235));
#43395=CARTESIAN_POINT('Ctrl Pts',(-20.3369746884962,23.7971858952935,3.95750383124104));
#43396=CARTESIAN_POINT('Ctrl Pts',(-20.3381917518322,23.812794432353,3.95849095884233));
#43397=CARTESIAN_POINT('Ctrl Pts',(-20.3391956584141,23.8248002882222,3.95924706665686));
#43398=CARTESIAN_POINT('Ctrl Pts',(-20.340583706471,23.8403495697253,3.96022196894315));
#43399=CARTESIAN_POINT('Ctrl Pts',(-20.3409064152843,23.8438981760711,3.96044416319671));
#43400=CARTESIAN_POINT('Ctrl Pts',(-20.3414101259311,23.8493371074322,3.96078425969256));
#43401=CARTESIAN_POINT('Ctrl Pts',(-20.3415869128891,23.851227805113,3.9609023999086));
#43402=CARTESIAN_POINT('Ctrl Pts',(-20.3419370785004,23.8549373748143,3.96113402374322));
#43403=CARTESIAN_POINT('Ctrl Pts',(-20.3421103319471,23.8567562462978,3.96124751349687));
#43404=CARTESIAN_POINT('Ctrl Pts',(-20.3424820801453,23.8606241323027,3.96148868377151));
#43405=CARTESIAN_POINT('Ctrl Pts',(-20.3426809907617,23.862673097843,3.96161634002559));
#43406=CARTESIAN_POINT('Ctrl Pts',(-20.3431081756265,23.8670300891329,3.96188758106753));
#43407=CARTESIAN_POINT('Ctrl Pts',(-20.3433369785467,23.8693380635095,3.96203113585575));
#43408=CARTESIAN_POINT('Ctrl Pts',(-20.3439261173171,23.8752161643368,3.96239643338741));
#43409=CARTESIAN_POINT('Ctrl Pts',(-20.3442899257933,23.8787859515027,3.96261798145719));
#43410=CARTESIAN_POINT('Ctrl Pts',(-20.3453526601469,23.8890439064318,3.96325377255932));
#43411=CARTESIAN_POINT('Ctrl Pts',(-20.3460665631807,23.8957305531389,3.96366718882883));
#43412=CARTESIAN_POINT('Ctrl Pts',(-20.3485304899675,23.9181437007368,3.96504964159991));
#43413=CARTESIAN_POINT('Ctrl Pts',(-20.3503754389167,23.9338598293908,3.96601358795155));
#43414=CARTESIAN_POINT('Ctrl Pts',(-20.3585526188446,23.9993477131949,3.97000998438442));
#43415=CARTESIAN_POINT('Ctrl Pts',(-20.3659312616306,24.0489843886988,3.97299012986646));
#43416=CARTESIAN_POINT('Ctrl Pts',(-20.3818638631928,24.1412873571795,3.97847394052762));
#43417=CARTESIAN_POINT('Ctrl Pts',(-20.3901283274464,24.1839908148912,3.98098757985366));
#43418=CARTESIAN_POINT('Ctrl Pts',(-20.4453666258353,24.4413696441169,3.99606445192876));
#43419=CARTESIAN_POINT('Ctrl Pts',(-20.5133331291118,24.6509502885966,4.00807066484408));
#43420=CARTESIAN_POINT('Ctrl Pts',(-20.6717987308724,25.0098398122419,4.0303154867419));
#43421=CARTESIAN_POINT('Ctrl Pts',(-20.7540493506933,25.1618126135886,4.04033648725274));
#43422=CARTESIAN_POINT('Ctrl Pts',(-20.854311140483,25.3160807320288,4.05152515961816));
#43423=CARTESIAN_POINT('Ctrl Pts',(-20.8606151263234,25.3256679310502,4.05222482607548));
#43424=CARTESIAN_POINT('Ctrl Pts',(-20.8694288159792,25.338917249863,4.0531978547721));
#43425=CARTESIAN_POINT('Ctrl Pts',(-20.871895143431,25.3426082355589,4.05346958144129));
#43426=CARTESIAN_POINT('Ctrl Pts',(-20.8761499152968,25.3489473280607,4.05393740255234));
#43427=CARTESIAN_POINT('Ctrl Pts',(-20.8779346915595,25.3515978996585,4.05413335809062));
#43428=CARTESIAN_POINT('Ctrl Pts',(-20.8816206269563,25.357054348965,4.05453746466929));
#43429=CARTESIAN_POINT('Ctrl Pts',(-20.8835222752581,25.3598598894239,4.05474563407942));
#43430=CARTESIAN_POINT('Ctrl Pts',(-20.8879488883533,25.3663684313172,4.05522947367786));
#43431=CARTESIAN_POINT('Ctrl Pts',(-20.8904771546482,25.3700691690357,4.05550526918002));
#43432=CARTESIAN_POINT('Ctrl Pts',(-20.8985173043973,25.381785352917,4.05638059725024));
#43433=CARTESIAN_POINT('Ctrl Pts',(-20.9040577243792,25.3897810662143,4.05698121768391));
#43434=CARTESIAN_POINT('Ctrl Pts',(-20.9987342331777,25.5251015873525,4.06720202409792));
#43435=CARTESIAN_POINT('Ctrl Pts',(-21.096915653646,25.6458191565422,4.07717744811887));
#43436=CARTESIAN_POINT('Ctrl Pts',(-21.2319959830646,25.7893470291109,4.09019124602269));
#43437=CARTESIAN_POINT('Ctrl Pts',(-21.2611708203737,25.819164678529,4.09296371721845));
#43438=CARTESIAN_POINT('Ctrl Pts',(-21.3172920720689,25.8743380074061,4.09822205952632));
#43439=CARTESIAN_POINT('Ctrl Pts',(-21.3441127154999,25.899812645873,4.10070444321883));
#43440=CARTESIAN_POINT('Ctrl Pts',(-21.5661230513116,26.1035278711038,4.12099008508655));
#43441=CARTESIAN_POINT('Ctrl Pts',(-21.7821357923939,26.2576066670105,4.139206332941));
#43442=CARTESIAN_POINT('Ctrl Pts',(-22.0179677358209,26.3854308282318,4.15616683921355));
#43443=CARTESIAN_POINT('Ctrl Pts',(-22.0213881378354,26.3872767357445,4.15641222829118));
#43444=CARTESIAN_POINT('Ctrl Pts',(-22.0352751995457,26.3947388363725,4.15740607305866));
#43445=CARTESIAN_POINT('Ctrl Pts',(-22.0457697075401,26.4003034254026,4.15815148661553));
#43446=CARTESIAN_POINT('Ctrl Pts',(-22.0594348432145,26.4074526891524,4.15911456945468));
#43447=CARTESIAN_POINT('Ctrl Pts',(-22.0625774768617,26.4090902416001,4.15933553887004));
#43448=CARTESIAN_POINT('Ctrl Pts',(-22.0674047988322,26.4115955301246,4.15967416709459));
#43449=CARTESIAN_POINT('Ctrl Pts',(-22.0690875492545,26.4124669625778,4.15979206065166));
#43450=CARTESIAN_POINT('Ctrl Pts',(-22.0721921739013,26.4140712585016,4.16000929574724));
#43451=CARTESIAN_POINT('Ctrl Pts',(-22.0736138177173,26.414804543736,4.16010866388677));
#43452=CARTESIAN_POINT('Ctrl Pts',(-22.0750360153459,26.4155367745562,4.16020796448761));
#43453=CARTESIAN_POINT('Origin',(-23.5502525316942,23.5502525316942,-77.3107734492734));
#43454=CARTESIAN_POINT('',(-22.0750360153137,26.4155367745396,5.65630390104212));
#43455=CARTESIAN_POINT('',(-22.0750360281848,26.4155367811664,5.40632238256859));
#43456=CARTESIAN_POINT('',(-22.0750360153461,26.4155367745563,-77.3107734492734));
#43457=CARTESIAN_POINT('Ctrl Pts',(-22.0750360153137,26.4155367745396,5.65630390104212));
#43458=CARTESIAN_POINT('Ctrl Pts',(-22.0290555371617,26.3918633253974,5.65326402867864));
#43459=CARTESIAN_POINT('Ctrl Pts',(-21.9836533856863,26.3670874447904,5.65019038681477));
#43460=CARTESIAN_POINT('Ctrl Pts',(-21.9220268220882,26.3315070678986,5.64590801223686));
#43461=CARTESIAN_POINT('Ctrl Pts',(-21.9052737229307,26.3216313311224,5.64473237729546));
#43462=CARTESIAN_POINT('Ctrl Pts',(-21.8770031911469,26.3046195638544,5.64272842066564));
#43463=CARTESIAN_POINT('Ctrl Pts',(-21.8654393787476,26.297561348404,5.64190294107446));
#43464=CARTESIAN_POINT('Ctrl Pts',(-21.8495744331906,26.2877400102614,5.64076231185462));
#43465=CARTESIAN_POINT('Ctrl Pts',(-21.8452347430775,26.2850391833485,5.64044946276797));
#43466=CARTESIAN_POINT('Ctrl Pts',(-21.8382460655568,26.2806666457264,5.63994428065526));
#43467=CARTESIAN_POINT('Ctrl Pts',(-21.8355930457878,26.2790013698037,5.63975218623473));
#43468=CARTESIAN_POINT('Ctrl Pts',(-21.8300692858842,26.2755229205012,5.63935156614846));
#43469=CARTESIAN_POINT('Ctrl Pts',(-21.8271989762515,26.2737090737028,5.6391430156384));
#43470=CARTESIAN_POINT('Ctrl Pts',(-21.8205784774395,26.2695106986353,5.63866111168083));
#43471=CARTESIAN_POINT('Ctrl Pts',(-21.8168303497589,26.2671229465827,5.63838763844325));
#43472=CARTESIAN_POINT('Ctrl Pts',(-21.8067944655993,26.2607003452975,5.63765364663537));
#43473=CARTESIAN_POINT('Ctrl Pts',(-21.80051580883,26.2566513895219,5.63719260179465));
#43474=CARTESIAN_POINT('Ctrl Pts',(-21.7564776375493,26.2280349233244,5.63394578047632));
#43475=CARTESIAN_POINT('Ctrl Pts',(-21.7192244018785,26.2027009408788,5.63113130114599));
#43476=CARTESIAN_POINT('Ctrl Pts',(-21.6813756207168,26.1757845942994,5.62819899730163));
#43477=CARTESIAN_POINT('Ctrl Pts',(-21.6802359199613,26.1749729724241,5.62811063084494));
#43478=CARTESIAN_POINT('Ctrl Pts',(-21.6687946382393,26.166813989787,5.62722283924283));
#43479=CARTESIAN_POINT('Ctrl Pts',(-21.658536002613,26.1594068458606,5.62642115899545));
#43480=CARTESIAN_POINT('Ctrl Pts',(-21.6451110695161,26.1495927143785,5.62536455012179));
#43481=CARTESIAN_POINT('Ctrl Pts',(-21.6419051279042,26.1472399329827,5.6251116611497));
#43482=CARTESIAN_POINT('Ctrl Pts',(-21.6346883916467,26.1419231241593,5.62454111795175));
#43483=CARTESIAN_POINT('Ctrl Pts',(-21.6306801125763,26.1389557131734,5.624223337541));
#43484=CARTESIAN_POINT('Ctrl Pts',(-21.6080008173527,26.1220841307784,5.62242022863408));
#43485=CARTESIAN_POINT('Ctrl Pts',(-21.5894743734467,26.1079875582406,5.62092775291979));
#43486=CARTESIAN_POINT('Ctrl Pts',(-21.3394783174193,25.9134558177032,5.60052000821524));
#43487=CARTESIAN_POINT('Ctrl Pts',(-21.1335827520115,25.7024383207263,5.58036746222942));
#43488=CARTESIAN_POINT('Ctrl Pts',(-20.9327473112214,25.4308780225437,5.55774902135405));
#43489=CARTESIAN_POINT('Ctrl Pts',(-20.907105669774,25.3946659202274,5.55479578657131));
#43490=CARTESIAN_POINT('Ctrl Pts',(-20.8494464113194,25.3095642213742,5.54801767184724));
#43491=CARTESIAN_POINT('Ctrl Pts',(-20.8179929185352,25.2603079844279,5.5442142317708));
#43492=CARTESIAN_POINT('Ctrl Pts',(-20.7737856529536,25.1867425264889,5.53873623290542));
#43493=CARTESIAN_POINT('Ctrl Pts',(-20.7599764333682,25.1630845904282,5.53700438566315));
#43494=CARTESIAN_POINT('Ctrl Pts',(-20.7442987529375,25.1354214014504,5.53501627526534));
#43495=CARTESIAN_POINT('Ctrl Pts',(-20.742135367224,25.1315858126066,5.53474143388893));
#43496=CARTESIAN_POINT('Ctrl Pts',(-20.7388576392711,25.1257466057406,5.53432427637956));
#43497=CARTESIAN_POINT('Ctrl Pts',(-20.7377375732026,25.1237462326153,5.53418159146706));
#43498=CARTESIAN_POINT('Ctrl Pts',(-20.7357103094844,25.120116576581,5.53392309830465));
#43499=CARTESIAN_POINT('Ctrl Pts',(-20.7348023943846,25.1184877067895,5.53380724372401));
#43500=CARTESIAN_POINT('Ctrl Pts',(-20.7329781361281,25.1152081562906,5.5335742823345));
#43501=CARTESIAN_POINT('Ctrl Pts',(-20.7320618333631,25.1135574650815,5.53345717825035));
#43502=CARTESIAN_POINT('Ctrl Pts',(-20.7294465949341,25.1088364219725,5.53312268746577));
#43503=CARTESIAN_POINT('Ctrl Pts',(-20.7277512159577,25.1057640870484,5.53290553066963));
#43504=CARTESIAN_POINT('Ctrl Pts',(-20.7204804460373,25.0925371056361,5.53197284326336));
#43505=CARTESIAN_POINT('Ctrl Pts',(-20.7149547217813,25.0823550421389,5.53126046884061));
#43506=CARTESIAN_POINT('Ctrl Pts',(-20.6208842135392,24.906762571205,5.51906760304813));
#43507=CARTESIAN_POINT('Ctrl Pts',(-20.5468806858322,24.7339325257884,5.50845904945429));
#43508=CARTESIAN_POINT('Ctrl Pts',(-20.3976991786451,24.2795893993786,5.48167090548814));
#43509=CARTESIAN_POINT('Ctrl Pts',(-20.3448158713582,23.9926108723074,5.46562888911613));
#43510=CARTESIAN_POINT('Ctrl Pts',(-20.330186488909,23.6831612581514,5.44698339788424));
#43511=CARTESIAN_POINT('Ctrl Pts',(-20.3294483047411,23.6638754004049,5.44581656451247));
#43512=CARTESIAN_POINT('Ctrl Pts',(-20.3286165705855,23.6354722421496,5.44409062720214));
#43513=CARTESIAN_POINT('Ctrl Pts',(-20.3283884041776,23.6263590761697,5.44353572553851));
#43514=CARTESIAN_POINT('Ctrl Pts',(-20.328046419847,23.6099111138717,5.44253211032834));
#43515=CARTESIAN_POINT('Ctrl Pts',(-20.3279189735424,23.6025766395024,5.44208382596923));
#43516=CARTESIAN_POINT('Ctrl Pts',(-20.3277610720437,23.5912666756295,5.44139137794753));
#43517=CARTESIAN_POINT('Ctrl Pts',(-20.3277129295015,23.5872914247429,5.4411477698532));
#43518=CARTESIAN_POINT('Ctrl Pts',(-20.3276378447444,23.5799732007256,5.44069888250149));
#43519=CARTESIAN_POINT('Ctrl Pts',(-20.3276087483241,23.576630251152,5.44049367116951));
#43520=CARTESIAN_POINT('Ctrl Pts',(-20.327560699023,23.5699079297802,5.44008068751993));
#43521=CARTESIAN_POINT('Ctrl Pts',(-20.3275418599535,23.5665285616103,5.43987291188821));
#43522=CARTESIAN_POINT('Ctrl Pts',(-20.3275033594944,23.5569077395582,5.43928091559561));
#43523=CARTESIAN_POINT('Ctrl Pts',(-20.327496514456,23.5506662749142,5.43889629300001));
#43524=CARTESIAN_POINT('Ctrl Pts',(-20.3275444873398,23.5241369006475,5.43725900987204));
#43525=CARTESIAN_POINT('Ctrl Pts',(-20.3277727487906,23.5038501201218,5.43600091680612));
#43526=CARTESIAN_POINT('Ctrl Pts',(-20.335385436394,23.1360249844661,5.41307611634389));
#43527=CARTESIAN_POINT('Ctrl Pts',(-20.3987641518351,22.7920002538353,5.38941409065657));
#43528=CARTESIAN_POINT('Ctrl Pts',(-20.5617834670544,22.3362375273107,5.35684324650837));
#43529=CARTESIAN_POINT('Ctrl Pts',(-20.6159303714036,22.2106471948495,5.34777554819578));
#43530=CARTESIAN_POINT('Ctrl Pts',(-20.6849828356838,22.0749249104377,5.3381457576323));
#43531=CARTESIAN_POINT('Ctrl Pts',(-20.6921742673289,22.0610411030107,5.33716279019482));
#43532=CARTESIAN_POINT('Ctrl Pts',(-20.7012072815686,22.0439083961411,5.33595295100066));
#43533=CARTESIAN_POINT('Ctrl Pts',(-20.7029536785057,22.0406099471909,5.3357201739217));
#43534=CARTESIAN_POINT('Ctrl Pts',(-20.7057138133191,22.0354186620876,5.33535405447914));
#43535=CARTESIAN_POINT('Ctrl Pts',(-20.7067237126433,22.0335238057401,5.33522046835777));
#43536=CARTESIAN_POINT('Ctrl Pts',(-20.7086152413127,22.0299832930941,5.33497096030692));
#43537=CARTESIAN_POINT('Ctrl Pts',(-20.7094964009972,22.0283374046735,5.33485500975453));
#43538=CARTESIAN_POINT('Ctrl Pts',(-20.7114782940145,22.0246432117581,5.33459484571123));
#43539=CARTESIAN_POINT('Ctrl Pts',(-20.712579811939,22.0225953367582,5.33445068353273));
#43540=CARTESIAN_POINT('Ctrl Pts',(-20.7153859646446,22.017391816128,5.33408452383512));
#43541=CARTESIAN_POINT('Ctrl Pts',(-20.7170936577156,22.0142378112623,5.33386272169738));
#43542=CARTESIAN_POINT('Ctrl Pts',(-20.7265508734569,21.9968403396303,5.33263998770461));
#43543=CARTESIAN_POINT('Ctrl Pts',(-20.7344027253136,21.9826523316972,5.33164550949222));
#43544=CARTESIAN_POINT('Ctrl Pts',(-20.8902436320566,21.7060029390145,5.31229517157563));
#43545=CARTESIAN_POINT('Ctrl Pts',(-21.0742377628744,21.4654685624687,5.29609217544438));
#43546=CARTESIAN_POINT('Ctrl Pts',(-21.4261247533412,21.1189501079005,5.2682346732949));
#43547=CARTESIAN_POINT('Ctrl Pts',(-21.5750374737539,20.9964986457951,5.25713202745246));
#43548=CARTESIAN_POINT('Ctrl Pts',(-21.7408270830447,20.8833880680165,5.24493138213758));
#43549=CARTESIAN_POINT('Ctrl Pts',(-21.7477048423628,20.8787345460701,5.24442557175939));
#43550=CARTESIAN_POINT('Ctrl Pts',(-21.7587089424675,20.8713509639663,5.24361679259769));
#43551=CARTESIAN_POINT('Ctrl Pts',(-21.7628237490258,20.8686037127524,5.24331447231518));
#43552=CARTESIAN_POINT('Ctrl Pts',(-21.7706609175496,20.8633972782554,5.24273886545928));
#43553=CARTESIAN_POINT('Ctrl Pts',(-21.7743820947898,20.8609363254668,5.24246564624699));
#43554=CARTESIAN_POINT('Ctrl Pts',(-21.7808980956154,20.8566464732773,5.24198736743706));
#43555=CARTESIAN_POINT('Ctrl Pts',(-21.7836906810652,20.8548141728779,5.24178243594389));
#43556=CARTESIAN_POINT('Ctrl Pts',(-21.7891329981473,20.8512553933314,5.24138314357982));
#43557=CARTESIAN_POINT('Ctrl Pts',(-21.7917824336377,20.8495284661049,5.24118879979639));
#43558=CARTESIAN_POINT('Ctrl Pts',(-21.7980518671788,20.8454551263698,5.24072901131145));
#43559=CARTESIAN_POINT('Ctrl Pts',(-21.8016740367922,20.8431120810594,5.24046344105088));
#43560=CARTESIAN_POINT('Ctrl Pts',(-21.8124507394307,20.8361716897949,5.23967352376699));
#43561=CARTESIAN_POINT('Ctrl Pts',(-21.8196187351081,20.8315954099799,5.23914839268551));
#43562=CARTESIAN_POINT('Ctrl Pts',(-21.8853170035304,20.7900166304407,5.2343376368014));
#43563=CARTESIAN_POINT('Ctrl Pts',(-21.9450035643996,20.7548836660666,5.22998336277636));
#43564=CARTESIAN_POINT('Ctrl Pts',(-22.0118386474232,20.7183895292736,5.22511951904495));
#43565=CARTESIAN_POINT('Ctrl Pts',(-22.0179161443742,20.7150963563418,5.22467734868954));
#43566=CARTESIAN_POINT('Ctrl Pts',(-22.0524727755572,20.6965149549662,5.22216379944567));
#43567=CARTESIAN_POINT('Ctrl Pts',(-22.0811692712005,20.6816367307315,5.22007889511683));
#43568=CARTESIAN_POINT('Ctrl Pts',(-22.2662981209989,20.5891597080422,5.20664450491016));
#43569=CARTESIAN_POINT('Ctrl Pts',(-22.4285790412283,20.5239601848639,5.19491685783022));
#43570=CARTESIAN_POINT('Ctrl Pts',(-22.7407280959838,20.4271185728184,5.17280071104562));
#43571=CARTESIAN_POINT('Ctrl Pts',(-22.8891555313429,20.3923654013195,5.16246598053466));
#43572=CARTESIAN_POINT('Ctrl Pts',(-23.0912842334221,20.3599206670471,5.14901764564463));
#43573=CARTESIAN_POINT('Ctrl Pts',(-23.1432769257045,20.3528722203996,5.14561404726355));
#43574=CARTESIAN_POINT('Ctrl Pts',(-23.2205167272727,20.3443159519055,5.14066182410012));
#43575=CARTESIAN_POINT('Ctrl Pts',(-23.2456445906256,20.3418309332545,5.1390670054621));
#43576=CARTESIAN_POINT('Ctrl Pts',(-23.2750935517111,20.339267687056,5.13721897508897));
#43577=CARTESIAN_POINT('Ctrl Pts',(-23.2793878802884,20.3389025853482,5.13695001332483));
#43578=CARTESIAN_POINT('Ctrl Pts',(-23.2859479490283,20.3383581038515,5.13653995629943));
#43579=CARTESIAN_POINT('Ctrl Pts',(-23.2882131466422,20.3381725064172,5.13639851110696));
#43580=CARTESIAN_POINT('Ctrl Pts',(-23.2923189361186,20.3378404734495,5.13614240458503));
#43581=CARTESIAN_POINT('Ctrl Pts',(-23.2941594508709,20.3376932239636,5.13602769753121));
#43582=CARTESIAN_POINT('Ctrl Pts',(-23.2981750167691,20.3373754333865,5.13577764915076));
#43583=CARTESIAN_POINT('Ctrl Pts',(-23.3003501090528,20.3372055196531,5.13564234402478));
#43584=CARTESIAN_POINT('Ctrl Pts',(-23.3062997386374,20.3367468248815,5.13527260934664));
#43585=CARTESIAN_POINT('Ctrl Pts',(-23.3100746300795,20.3364624842762,5.13503843095937));
#43586=CARTESIAN_POINT('Ctrl Pts',(-23.3283848193395,20.3351157253471,5.13390448948218));
#43587=CARTESIAN_POINT('Ctrl Pts',(-23.3429270108216,20.3341452398496,5.13300984354642));
#43588=CARTESIAN_POINT('Ctrl Pts',(-23.3662675889,20.3327465596985,5.13158273320885));
#43589=CARTESIAN_POINT('Ctrl Pts',(-23.3750618034998,20.3322557399463,5.13104703607255));
#43590=CARTESIAN_POINT('Ctrl Pts',(-23.3890978778253,20.331530072483,5.13019507672205));
#43591=CARTESIAN_POINT('Ctrl Pts',(-23.3943384161776,20.3312719661663,5.12987766419658));
#43592=CARTESIAN_POINT('Ctrl Pts',(-23.4040760662025,20.3308162043299,5.12928908627256));
#43593=CARTESIAN_POINT('Ctrl Pts',(-23.408572997435,20.3306151708916,5.12901775863018));
#43594=CARTESIAN_POINT('Ctrl Pts',(-23.7270422535201,20.3170466540945,5.10983579494653));
#43595=CARTESIAN_POINT('Ctrl Pts',(-24.0413303099646,20.349661198246,5.0930587851589));
#43596=CARTESIAN_POINT('Ctrl Pts',(-24.5040104236033,20.4675484386213,5.06591717534581));
#43597=CARTESIAN_POINT('Ctrl Pts',(-24.6587521119003,20.5197516086665,5.05642006923913));
#43598=CARTESIAN_POINT('Ctrl Pts',(-24.8164123223943,20.5866357975897,5.04600784111712));
#43599=CARTESIAN_POINT('Ctrl Pts',(-24.8239465692147,20.5898660266766,5.04550848197663));
#43600=CARTESIAN_POINT('Ctrl Pts',(-24.8359676781115,20.595074335915,5.04470885698203));
#43601=CARTESIAN_POINT('Ctrl Pts',(-24.8404625260121,20.5970339863307,5.04440922035229));
#43602=CARTESIAN_POINT('Ctrl Pts',(-24.8490089892762,20.6007832837076,5.04383825446901));
#43603=CARTESIAN_POINT('Ctrl Pts',(-24.8530614252034,20.6025710415036,5.04356699037738));
#43604=CARTESIAN_POINT('Ctrl Pts',(-24.8601584391799,20.6057194283309,5.04309098844088));
#43605=CARTESIAN_POINT('Ctrl Pts',(-24.8632046216483,20.6070764423958,5.04288637504695));
#43606=CARTESIAN_POINT('Ctrl Pts',(-24.8691433252045,20.6097330719735,5.04248687455178));
#43607=CARTESIAN_POINT('Ctrl Pts',(-24.8720360462252,20.6110322339288,5.0422920032373));
#43608=CARTESIAN_POINT('Ctrl Pts',(-24.8788894803211,20.6141223717511,5.04182965689296));
#43609=CARTESIAN_POINT('Ctrl Pts',(-24.8828484896799,20.6159170924753,5.04156205293057));
#43610=CARTESIAN_POINT('Ctrl Pts',(-24.8967453885571,20.622250838815,5.04062086880987));
#43611=CARTESIAN_POINT('Ctrl Pts',(-24.906663731159,20.6268323463075,5.03994582220136));
#43612=CARTESIAN_POINT('Ctrl Pts',(-25.0373620401496,20.6880131703327,5.03100608141913));
#43613=CARTESIAN_POINT('Ctrl Pts',(-25.1545219503958,20.7519994833869,5.02248222370348));
#43614=CARTESIAN_POINT('Ctrl Pts',(-25.3706010190642,20.8880484953357,5.00573566859235));
#43615=CARTESIAN_POINT('Ctrl Pts',(-25.4700511072598,20.9588497801394,4.99756392347781));
#43616=CARTESIAN_POINT('Ctrl Pts',(-25.6460484699152,21.0998489906195,4.98233287291109));
#43617=CARTESIAN_POINT('Ctrl Pts',(-25.7236879971006,21.1684430141461,4.97530196190845));
#43618=CARTESIAN_POINT('Ctrl Pts',(-25.9045459749293,21.3444491977166,4.95831929563578));
#43619=CARTESIAN_POINT('Ctrl Pts',(-26.0038989482285,21.4555216162748,4.94845129954147));
#43620=CARTESIAN_POINT('Ctrl Pts',(-26.0989786277632,21.5779061583656,4.93874057827075));
#43621=CARTESIAN_POINT('Ctrl Pts',(-26.1027151738623,21.5827441096125,4.93835849648739));
#43622=CARTESIAN_POINT('Ctrl Pts',(-26.1080344848724,21.589672027119,4.9378139457162));
#43623=CARTESIAN_POINT('Ctrl Pts',(-26.1096284704087,21.5917533003002,4.93765068508991));
#43624=CARTESIAN_POINT('Ctrl Pts',(-26.112377890287,21.5953523173932,4.93736894570905));
#43625=CARTESIAN_POINT('Ctrl Pts',(-26.1135345182704,21.596869144239,4.93725038171775));
#43626=CARTESIAN_POINT('Ctrl Pts',(-26.1157571557458,21.5997893322908,4.93702246394916));
#43627=CARTESIAN_POINT('Ctrl Pts',(-26.1168233587415,21.6011925382501,4.93691309619673));
#43628=CARTESIAN_POINT('Ctrl Pts',(-26.1193452833312,21.6045172446503,4.93665431976844));
#43629=CARTESIAN_POINT('Ctrl Pts',(-26.1208000035252,21.6064395085581,4.93650498242177));
#43630=CARTESIAN_POINT('Ctrl Pts',(-26.1251290179056,21.6121732165407,4.93606037090477));
#43631=CARTESIAN_POINT('Ctrl Pts',(-26.1279970180763,21.6159894382424,4.93576553947387));
#43632=CARTESIAN_POINT('Ctrl Pts',(-26.1544293316378,21.6513240342288,4.93304560853889));
#43633=CARTESIAN_POINT('Ctrl Pts',(-26.1774242540994,21.6832669056302,4.9306596288548));
#43634=CARTESIAN_POINT('Ctrl Pts',(-26.2013314149635,21.7177937252179,4.92814801068477));
#43635=CARTESIAN_POINT('Ctrl Pts',(-26.2028306307508,21.7199645895263,4.92799037346223));
#43636=CARTESIAN_POINT('Ctrl Pts',(-26.2052099989216,21.7234189783084,4.92773997391076));
#43637=CARTESIAN_POINT('Ctrl Pts',(-26.2060918869853,21.7247012989241,4.9276471182486));
#43638=CARTESIAN_POINT('Ctrl Pts',(-26.2086824577383,21.7284740016877,4.92737421023122));
#43639=CARTESIAN_POINT('Ctrl Pts',(-26.2103885734747,21.7309661541735,4.9271942946592));
#43640=CARTESIAN_POINT('Ctrl Pts',(-26.212699850902,21.7343524791958,4.92695030992237));
#43641=CARTESIAN_POINT('Ctrl Pts',(-26.21330806485,21.7352445549524,4.92688608135389));
#43642=CARTESIAN_POINT('Ctrl Pts',(-26.2211933398391,21.7468224929417,4.92605306897446));
#43643=CARTESIAN_POINT('Ctrl Pts',(-26.2284065802359,21.757551885379,4.92528760026367));
#43644=CARTESIAN_POINT('Ctrl Pts',(-26.3061491382792,21.8747071788135,4.9169963472863));
#43645=CARTESIAN_POINT('Ctrl Pts',(-26.3703653350986,21.9852005364838,4.90977191484756));
#43646=CARTESIAN_POINT('Ctrl Pts',(-26.504256639869,22.250726635808,4.89309453095971));
#43647=CARTESIAN_POINT('Ctrl Pts',(-26.5685665813311,22.4080237845715,4.88370645766961));
#43648=CARTESIAN_POINT('Ctrl Pts',(-26.6620330440601,22.7006365055362,4.86617276207587));
#43649=CARTESIAN_POINT('Ctrl Pts',(-26.69544182781,22.834150200173,4.85815043511401));
#43650=CARTESIAN_POINT('Ctrl Pts',(-26.7241250121101,22.9906811892552,4.84853131314228));
#43651=CARTESIAN_POINT('Ctrl Pts',(-26.7278136820209,23.0120223675674,4.8472155502313));
#43652=CARTESIAN_POINT('Ctrl Pts',(-26.732269638324,23.0394470464099,4.84551869918875));
#43653=CARTESIAN_POINT('Ctrl Pts',(-26.7332351137378,23.0454981436314,4.84514392431726));
#43654=CARTESIAN_POINT('Ctrl Pts',(-26.7347604235763,23.0552364132254,4.84454016959271));
#43655=CARTESIAN_POINT('Ctrl Pts',(-26.7353311287924,23.0589218883134,4.84431153546012));
#43656=CARTESIAN_POINT('Ctrl Pts',(-26.7364042233459,23.0659321143345,4.84387637308583));
#43657=CARTESIAN_POINT('Ctrl Pts',(-26.7369078093782,23.0692566793643,4.84366988315518));
#43658=CARTESIAN_POINT('Ctrl Pts',(-26.7380416995014,23.0768223170557,4.84319971136168));
#43659=CARTESIAN_POINT('Ctrl Pts',(-26.7386687437839,23.0810638652481,4.84293592640924));
#43660=CARTESIAN_POINT('Ctrl Pts',(-26.740546863439,23.0939457703661,4.84213420442753));
#43661=CARTESIAN_POINT('Ctrl Pts',(-26.7417712870527,23.1025899183498,4.8415954232885));
#43662=CARTESIAN_POINT('Ctrl Pts',(-26.7501669242444,23.1636468294434,4.83778402024732));
#43663=CARTESIAN_POINT('Ctrl Pts',(-26.7560814213144,23.2162215726421,4.83447182341248));
#43664=CARTESIAN_POINT('Ctrl Pts',(-26.7609921848854,23.2722602402259,4.8309064196588));
#43665=CARTESIAN_POINT('Ctrl Pts',(-26.7612800494691,23.2756052767537,4.8306934637042));
#43666=CARTESIAN_POINT('Ctrl Pts',(-26.76190666116,23.283022273614,4.83022098144621));
#43667=CARTESIAN_POINT('Ctrl Pts',(-26.7622428919642,23.2870944357958,4.82996137891756));
#43668=CARTESIAN_POINT('Ctrl Pts',(-26.762977164163,23.2961984499482,4.82938055593241));
#43669=CARTESIAN_POINT('Ctrl Pts',(-26.7633711294963,23.3012306119322,4.82905921282184));
#43670=CARTESIAN_POINT('Ctrl Pts',(-26.7652625168005,23.3261414792106,4.82746697708172));
#43671=CARTESIAN_POINT('Ctrl Pts',(-26.7665872666799,23.3460325206587,4.82619092464468));
#43672=CARTESIAN_POINT('Ctrl Pts',(-26.7712907986619,23.4281377467265,4.82090435995079));
#43673=CARTESIAN_POINT('Ctrl Pts',(-26.7730494221322,23.4904281366185,4.81684749405692));
#43674=CARTESIAN_POINT('Ctrl Pts',(-26.7728738638164,23.7190449075866,4.80179839398118));
#43675=CARTESIAN_POINT('Ctrl Pts',(-26.7598714911795,23.8850910761752,4.79054155792165));
#43676=CARTESIAN_POINT('Ctrl Pts',(-26.7046678499917,24.2372295273084,4.76642026884124));
#43677=CARTESIAN_POINT('Ctrl Pts',(-26.6586472059406,24.422132350987,4.75360217753736));
#43678=CARTESIAN_POINT('Ctrl Pts',(-26.5928181251123,24.6128179118957,4.74088904000005));
#43679=CARTESIAN_POINT('Ctrl Pts',(-26.5889959887278,24.6236996842783,4.74016542431284));
#43680=CARTESIAN_POINT('Ctrl Pts',(-26.5839368683926,24.6378596199334,4.73922649037708));
#43681=CARTESIAN_POINT('Ctrl Pts',(-26.5827529032909,24.6411564365647,4.73900807061101));
#43682=CARTESIAN_POINT('Ctrl Pts',(-26.5809229718887,24.6462259826305,4.73867250345071));
#43683=CARTESIAN_POINT('Ctrl Pts',(-26.5802808249788,24.6480000728728,4.7385551279544));
#43684=CARTESIAN_POINT('Ctrl Pts',(-26.5790008517,24.6515266367752,4.738321920794));
#43685=CARTESIAN_POINT('Ctrl Pts',(-26.5783630657773,24.6532791106429,4.73820608803403));
#43686=CARTESIAN_POINT('Ctrl Pts',(-26.5769371308502,24.6571866603517,4.73794793633169));
#43687=CARTESIAN_POINT('Ctrl Pts',(-26.5761482030211,24.6593414434949,4.73780566516316));
#43688=CARTESIAN_POINT('Ctrl Pts',(-26.5738351766597,24.6656381285636,4.73739016317186));
#43689=CARTESIAN_POINT('Ctrl Pts',(-26.5723048627207,24.6697777657684,4.73711730472283));
#43690=CARTESIAN_POINT('Ctrl Pts',(-26.5611331777055,24.6998083560886,4.73514000986864));
#43691=CARTESIAN_POINT('Ctrl Pts',(-26.5511673484998,24.7255785477257,4.73345473584688));
#43692=CARTESIAN_POINT('Ctrl Pts',(-26.5182457692878,24.8075591282002,4.72812076936408));
#43693=CARTESIAN_POINT('Ctrl Pts',(-26.4940314243791,24.8632531294324,4.72453841268557));
#43694=CARTESIAN_POINT('Ctrl Pts',(-26.4327737006213,24.993920367541,4.71615734955104));
#43695=CARTESIAN_POINT('Ctrl Pts',(-26.3943578097896,25.0682023802709,4.71141163070593));
#43696=CARTESIAN_POINT('Ctrl Pts',(-26.2248077437541,25.366960688579,4.69208098872679));
#43697=CARTESIAN_POINT('Ctrl Pts',(-26.0696568834325,25.5766459522074,4.67784024595707));
#43698=CARTESIAN_POINT('Ctrl Pts',(-25.8812510433842,25.7757333938321,4.66175717873313));
#43699=CARTESIAN_POINT('Ctrl Pts',(-25.8714244664303,25.7859805943172,4.66092161527053));
#43700=CARTESIAN_POINT('Ctrl Pts',(-25.8563325505458,25.8015117669704,4.6596430300755));
#43701=CARTESIAN_POINT('Ctrl Pts',(-25.8511159715902,25.8068430190046,4.65920192621688));
#43702=CARTESIAN_POINT('Ctrl Pts',(-25.8430355354815,25.8150439340495,4.65851992207102));
#43703=CARTESIAN_POINT('Ctrl Pts',(-25.8401846714975,25.8179264045258,4.65827954444316));
#43704=CARTESIAN_POINT('Ctrl Pts',(-25.8331939464501,25.8249680075673,4.65769068327534));
#43705=CARTESIAN_POINT('Ctrl Pts',(-25.8290481602912,25.8291212163322,4.65734195924947));
#43706=CARTESIAN_POINT('Ctrl Pts',(-25.8200006873544,25.8381355114466,4.65658197878899));
#43707=CARTESIAN_POINT('Ctrl Pts',(-25.8150946862768,25.842992210096,4.6561705447233));
#43708=CARTESIAN_POINT('Ctrl Pts',(-25.8021284008394,25.8557459634982,4.65508485237189));
#43709=CARTESIAN_POINT('Ctrl Pts',(-25.7940422288221,25.8636164642438,4.65440950463946));
#43710=CARTESIAN_POINT('Ctrl Pts',(-25.7785660685551,25.8785223721214,4.65312008545666));
#43711=CARTESIAN_POINT('Ctrl Pts',(-25.7711836651245,25.8855654797503,4.65250634758203));
#43712=CARTESIAN_POINT('Ctrl Pts',(-25.7587709168142,25.8972956450653,4.65147655987787));
#43713=CARTESIAN_POINT('Ctrl Pts',(-25.7537587613022,25.9020019078812,4.65106132137479));
#43714=CARTESIAN_POINT('Ctrl Pts',(-25.7342222249319,25.9202288413031,4.64944498706106));
#43715=CARTESIAN_POINT('Ctrl Pts',(-25.7195883800787,25.9336310745619,4.64823895972118));
#43716=CARTESIAN_POINT('Ctrl Pts',(-25.7002306869885,25.9510336080784,4.64664932794436));
#43717=CARTESIAN_POINT('Ctrl Pts',(-25.695617547597,25.9551568525902,4.64627092183977));
#43718=CARTESIAN_POINT('Ctrl Pts',(-25.6884746234795,25.9615043218462,4.64568563677741));
#43719=CARTESIAN_POINT('Ctrl Pts',(-25.6859531597954,25.963737923467,4.64547915157451));
#43720=CARTESIAN_POINT('Ctrl Pts',(-25.6809216515002,25.9681809521242,4.64506735530463));
#43721=CARTESIAN_POINT('Ctrl Pts',(-25.6784116606679,25.9703904339737,4.64486204689995));
#43722=CARTESIAN_POINT('Ctrl Pts',(-25.6728350940495,25.9752839616992,4.64440616231671));
#43723=CARTESIAN_POINT('Ctrl Pts',(-25.669766860549,25.9779661021267,4.64415550716968));
#43724=CARTESIAN_POINT('Ctrl Pts',(-25.6608848587447,25.9857007595265,4.64343039759552));
#43725=CARTESIAN_POINT('Ctrl Pts',(-25.6550580835287,25.990738236991,4.64295531970268));
#43726=CARTESIAN_POINT('Ctrl Pts',(-25.6152661146684,26.0248914603937,4.63971498098456));
#43727=CARTESIAN_POINT('Ctrl Pts',(-25.5807173447519,26.0533169021919,4.63692147590551));
#43728=CARTESIAN_POINT('Ctrl Pts',(-25.5133910569373,26.1063992205342,4.63151163056614));
#43729=CARTESIAN_POINT('Ctrl Pts',(-25.4807123533074,26.1311677561835,4.62890046004988));
#43730=CARTESIAN_POINT('Ctrl Pts',(-25.4001135059712,26.1898697143194,4.62249427694327));
#43731=CARTESIAN_POINT('Ctrl Pts',(-25.3517226398677,26.2231291252522,4.61867617752031));
#43732=CARTESIAN_POINT('Ctrl Pts',(-25.1648488703491,26.3441883273632,4.60404347867693));
#43733=CARTESIAN_POINT('Ctrl Pts',(-25.0206538164229,26.4226922844705,4.5929627316583));
#43734=CARTESIAN_POINT('Ctrl Pts',(-24.6914382558783,26.5706199987887,4.56853267147059));
#43735=CARTESIAN_POINT('Ctrl Pts',(-24.5047018269214,26.6347250000079,4.55522316539849));
#43736=CARTESIAN_POINT('Ctrl Pts',(-24.3017498118959,26.6841813365457,4.54205476130365));
#43737=CARTESIAN_POINT('Ctrl Pts',(-24.2902239540649,26.6869227758382,4.54131131455393));
#43738=CARTESIAN_POINT('Ctrl Pts',(-24.2752347193874,26.690400764033,4.54035041488178));
#43739=CARTESIAN_POINT('Ctrl Pts',(-24.271785073716,26.6911952062146,4.54012967996918));
#43740=CARTESIAN_POINT('Ctrl Pts',(-24.2664875482689,26.6924060211721,4.53979133706199));
#43741=CARTESIAN_POINT('Ctrl Pts',(-24.2646406128451,26.6928264480817,4.53967349492698));
#43742=CARTESIAN_POINT('Ctrl Pts',(-24.2610112214233,26.6936492592026,4.53944215822162));
#43743=CARTESIAN_POINT('Ctrl Pts',(-24.2592288033286,26.6940517536276,4.53932865803515));
#43744=CARTESIAN_POINT('Ctrl Pts',(-24.2552815007607,26.6949395809058,4.53907754786697));
#43745=CARTESIAN_POINT('Ctrl Pts',(-24.2531164623426,26.695424193109,4.53893998024437));
#43746=CARTESIAN_POINT('Ctrl Pts',(-24.2486159006409,26.6964266988772,4.53865434704681));
#43747=CARTESIAN_POINT('Ctrl Pts',(-24.2462802964862,26.6969442287092,4.5385063025294));
#43748=CARTESIAN_POINT('Ctrl Pts',(-24.2402701815356,26.6982689482508,4.53812582207067));
#43749=CARTESIAN_POINT('Ctrl Pts',(-24.2365948167534,26.6990723080676,4.53789360482869));
#43750=CARTESIAN_POINT('Ctrl Pts',(-24.2259019861915,26.7013899318327,4.53721931834472));
#43751=CARTESIAN_POINT('Ctrl Pts',(-24.2188808014586,26.7028871979796,4.53677820290706));
#43752=CARTESIAN_POINT('Ctrl Pts',(-24.1466024868981,26.7180482117521,4.53225351255114));
#43753=CARTESIAN_POINT('Ctrl Pts',(-24.0809358601629,26.7297083681593,4.52827915837504));
#43754=CARTESIAN_POINT('Ctrl Pts',(-23.9716544494525,26.7456323605316,4.52181952275864));
#43755=CARTESIAN_POINT('Ctrl Pts',(-23.9282337729237,26.7510590374859,4.51929287418227));
#43756=CARTESIAN_POINT('Ctrl Pts',(-23.6126085754082,26.7839929516179,4.5011314005564));
#43757=CARTESIAN_POINT('Ctrl Pts',(-23.3379951139738,26.7776237154805,4.48632970877388));
#43758=CARTESIAN_POINT('Ctrl Pts',(-22.9505806139728,26.718925663682,4.46370097501754));
#43759=CARTESIAN_POINT('Ctrl Pts',(-22.8347606885478,26.6947973756382,4.45672095188124));
#43760=CARTESIAN_POINT('Ctrl Pts',(-22.7102627019604,26.6616264564022,4.4488812256495));
#43761=CARTESIAN_POINT('Ctrl Pts',(-22.7000022920564,26.6588382453509,4.44823262611958));
#43762=CARTESIAN_POINT('Ctrl Pts',(-22.6856155102209,26.654852158533,4.44731961575147));
#43763=CARTESIAN_POINT('Ctrl Pts',(-22.6814773713433,26.6536967058878,4.44705658683998));
#43764=CARTESIAN_POINT('Ctrl Pts',(-22.6743015504593,26.6516775935641,4.44659975071053));
#43765=CARTESIAN_POINT('Ctrl Pts',(-22.6712627968822,26.6508177353158,4.44640606765432));
#43766=CARTESIAN_POINT('Ctrl Pts',(-22.6649438438396,26.6490196622944,4.44600283966205));
#43767=CARTESIAN_POINT('Ctrl Pts',(-22.6616638623614,26.648080703022,4.4457932706497));
#43768=CARTESIAN_POINT('Ctrl Pts',(-22.6539459394565,26.6458580295738,4.44529951894137));
#43769=CARTESIAN_POINT('Ctrl Pts',(-22.6495092638769,26.6445699800046,4.44501519482447));
#43770=CARTESIAN_POINT('Ctrl Pts',(-22.6350213756625,26.6403300766814,4.44408513023094));
#43771=CARTESIAN_POINT('Ctrl Pts',(-22.6249818624688,26.6373387772528,4.44343809971391));
#43772=CARTESIAN_POINT('Ctrl Pts',(-22.6015601153087,26.6302356892728,4.44192260319975));
#43773=CARTESIAN_POINT('Ctrl Pts',(-22.5881898145426,26.6260855684775,4.44105288657199));
#43774=CARTESIAN_POINT('Ctrl Pts',(-22.447979695722,26.5815609286362,4.43188337308708));
#43775=CARTESIAN_POINT('Ctrl Pts',(-22.3237470330152,26.5334575321492,4.42332742690915));
#43776=CARTESIAN_POINT('Ctrl Pts',(-22.1597826851877,26.4579938422594,4.41143761695813));
#43777=CARTESIAN_POINT('Ctrl Pts',(-22.1171657233614,26.437227623864,4.40829071839276));
#43778=CARTESIAN_POINT('Ctrl Pts',(-22.07503587195,26.4155367007276,4.4051257859302));
#43779=CARTESIAN_POINT('',(-26.7730023406925,23.55136208175,4.56709764253913));
#43780=CARTESIAN_POINT('Ctrl Pts',(-22.0750360153459,26.4155367745562,4.16020796448761));
#43781=CARTESIAN_POINT('Ctrl Pts',(-22.0752387407196,26.4156411494782,4.16022211916697));
#43782=CARTESIAN_POINT('Ctrl Pts',(-22.0754414773459,26.4157455029758,4.16023627247669));
#43783=CARTESIAN_POINT('Ctrl Pts',(-22.0776159214908,26.416864450636,4.1603880501777));
#43784=CARTESIAN_POINT('Ctrl Pts',(-22.0795886715041,26.4178770346465,4.16052554583761));
#43785=CARTESIAN_POINT('Ctrl Pts',(-22.0836906523566,26.4199771757902,4.16081102372231));
#43786=CARTESIAN_POINT('Ctrl Pts',(-22.0858200526079,26.4210644017309,4.16095898492431));
#43787=CARTESIAN_POINT('Ctrl Pts',(-22.0913002370208,26.4238547819672,4.16133917685715));
#43788=CARTESIAN_POINT('Ctrl Pts',(-22.0946528062336,26.4255544515772,4.16157118936666));
#43789=CARTESIAN_POINT('Ctrl Pts',(-22.1044091483979,26.4304792385287,4.16224472436418));
#43790=CARTESIAN_POINT('Ctrl Pts',(-22.1108207707646,26.4336888808583,4.16268529564305));
#43791=CARTESIAN_POINT('Ctrl Pts',(-22.1327027364086,26.4445517629403,4.16418208068455));
#43792=CARTESIAN_POINT('Ctrl Pts',(-22.1482241388819,26.4521022654713,4.1652322024229));
#43793=CARTESIAN_POINT('Ctrl Pts',(-22.2083525987552,26.4807571345579,4.16925860410626));
#43794=CARTESIAN_POINT('Ctrl Pts',(-22.2533836975093,26.5009616750483,4.17218613963835));
#43795=CARTESIAN_POINT('Ctrl Pts',(-22.3391706292074,26.5371089552848,4.17763153981386));
#43796=CARTESIAN_POINT('Ctrl Pts',(-22.3798207474081,26.5532710776522,4.18015753756762));
#43797=CARTESIAN_POINT('Ctrl Pts',(-22.6756495243272,26.663969985544,4.1982352214823));
#43798=CARTESIAN_POINT('Ctrl Pts',(-22.9415623312482,26.7266774940453,4.21296121383391));
#43799=CARTESIAN_POINT('Ctrl Pts',(-23.3312794697115,26.7677834330629,4.23557914435609));
#43800=CARTESIAN_POINT('Ctrl Pts',(-23.4509495709218,26.7736960440887,4.24264498599362));
#43801=CARTESIAN_POINT('Ctrl Pts',(-23.5813261939395,26.7728703687676,4.25057811817322));
#43802=CARTESIAN_POINT('Ctrl Pts',(-23.5919900823455,26.7727498969192,4.25122866390271));
#43803=CARTESIAN_POINT('Ctrl Pts',(-23.6069546422885,26.7725065473661,4.25214397694664));
#43804=CARTESIAN_POINT('Ctrl Pts',(-23.611256046848,26.7724279834203,4.25240735307333));
#43805=CARTESIAN_POINT('Ctrl Pts',(-23.6187162658897,26.7722767809801,4.25286463289879));
#43806=CARTESIAN_POINT('Ctrl Pts',(-23.6218751626426,26.7722081093698,4.25305841186525));
#43807=CARTESIAN_POINT('Ctrl Pts',(-23.6284439736687,26.772055644155,4.25346168635388));
#43808=CARTESIAN_POINT('Ctrl Pts',(-23.6318538642192,26.7719710823206,4.25367120572753));
#43809=CARTESIAN_POINT('Ctrl Pts',(-23.6398763955407,26.7717593869084,4.25416456945638));
#43810=CARTESIAN_POINT('Ctrl Pts',(-23.6444889011699,26.7716277599899,4.25444855457217));
#43811=CARTESIAN_POINT('Ctrl Pts',(-23.659540675307,26.7711658729303,4.25537635210081));
#43812=CARTESIAN_POINT('Ctrl Pts',(-23.6699785423175,26.7707947730481,4.25602144576727));
#43813=CARTESIAN_POINT('Ctrl Pts',(-23.8643721546152,26.7629371100988,4.26806783752885));
#43814=CARTESIAN_POINT('Ctrl Pts',(-24.0473203545893,26.7397533572145,4.27997342002075));
#43815=CARTESIAN_POINT('Ctrl Pts',(-24.260708956705,26.6939031933505,4.29451153138907));
#43816=CARTESIAN_POINT('Ctrl Pts',(-24.2940373918442,26.6861848990009,4.29680047082384));
#43817=CARTESIAN_POINT('Ctrl Pts',(-24.3544600926756,26.6711746147513,4.30098081816748));
#43818=CARTESIAN_POINT('Ctrl Pts',(-24.3815943797773,26.6640564991932,4.30286945473942));
#43819=CARTESIAN_POINT('Ctrl Pts',(-24.4315831867193,26.6502429863717,4.30636795784229));
#43820=CARTESIAN_POINT('Ctrl Pts',(-24.4544632524606,26.6436467035083,4.30797670944009));
#43821=CARTESIAN_POINT('Ctrl Pts',(-24.4970560720837,26.6308543410923,4.31098412268456));
#43822=CARTESIAN_POINT('Ctrl Pts',(-24.5167865045487,26.6247210268544,4.31238235728614));
#43823=CARTESIAN_POINT('Ctrl Pts',(-24.5933426779191,26.6001133294704,4.31782544752065));
#43824=CARTESIAN_POINT('Ctrl Pts',(-24.6497097583347,26.5802495398251,4.32187170621528));
#43825=CARTESIAN_POINT('Ctrl Pts',(-24.7855595310423,26.5280856599102,4.33168074718154));
#43826=CARTESIAN_POINT('Ctrl Pts',(-24.864372231619,26.4941554877538,4.33742074381131));
#43827=CARTESIAN_POINT('Ctrl Pts',(-25.0068983713246,26.4259296193237,4.34778868621606));
#43828=CARTESIAN_POINT('Ctrl Pts',(-25.0709945763356,26.3925546609894,4.35244612598531));
#43829=CARTESIAN_POINT('Ctrl Pts',(-25.1392279096219,26.3540556542697,4.35735575495317));
#43830=CARTESIAN_POINT('Ctrl Pts',(-25.1445270968971,26.3510458682359,4.35773672433705));
#43831=CARTESIAN_POINT('Ctrl Pts',(-25.1519218232155,26.3468180891671,4.35826785556285));
#43832=CARTESIAN_POINT('Ctrl Pts',(-25.1540245311552,26.3456127608034,4.35841882836347));
#43833=CARTESIAN_POINT('Ctrl Pts',(-25.1576568130177,26.343525192353,4.35867952448024));
#43834=CARTESIAN_POINT('Ctrl Pts',(-25.1591870212652,26.3426440674042,4.35878932018916));
#43835=CARTESIAN_POINT('Ctrl Pts',(-25.162333569468,26.3408287760119,4.35901502794548));
#43836=CARTESIAN_POINT('Ctrl Pts',(-25.1639498196787,26.3398944639978,4.35913092972764));
#43837=CARTESIAN_POINT('Ctrl Pts',(-25.1676264146596,26.3377648561393,4.35939450200822));
#43838=CARTESIAN_POINT('Ctrl Pts',(-25.1696862528947,26.3365686765279,4.35954211486434));
#43839=CARTESIAN_POINT('Ctrl Pts',(-25.1741187642971,26.3339880735976,4.35985964395077));
#43840=CARTESIAN_POINT('Ctrl Pts',(-25.1764909996853,26.3326028967634,4.36002951116732));
#43841=CARTESIAN_POINT('Ctrl Pts',(-25.1828429889173,26.3288829948421,4.36048417140519));
#43842=CARTESIAN_POINT('Ctrl Pts',(-25.1868195233418,26.3265427424281,4.36076860966511));
#43843=CARTESIAN_POINT('Ctrl Pts',(-25.1989626343907,26.3193611771279,4.36163665015468));
#43844=CARTESIAN_POINT('Ctrl Pts',(-25.2071129445719,26.3144922590636,4.36221851109815));
#43845=CARTESIAN_POINT('Ctrl Pts',(-25.2368764486304,26.2965328896313,4.36434103613836));
#43846=CARTESIAN_POINT('Ctrl Pts',(-25.2583576327798,26.2832240086095,4.36586840690217));
#43847=CARTESIAN_POINT('Ctrl Pts',(-25.3422431597206,26.2298764239828,4.37182412473616));
#43848=CARTESIAN_POINT('Ctrl Pts',(-25.4034186368347,26.1879393256783,4.37614832515994));
#43849=CARTESIAN_POINT('Ctrl Pts',(-25.7742899928164,25.9144202370695,4.40259814194256));
#43850=CARTESIAN_POINT('Ctrl Pts',(-26.0416315412958,25.6308046367301,4.42315569072723));
#43851=CARTESIAN_POINT('Ctrl Pts',(-26.2633105935426,25.2897454905011,4.44775990615106));
#43852=CARTESIAN_POINT('Ctrl Pts',(-26.27408307747,25.2728281992097,4.44897874543893));
#43853=CARTESIAN_POINT('Ctrl Pts',(-26.2879851189343,25.2505396989263,4.45058290608779));
#43854=CARTESIAN_POINT('Ctrl Pts',(-26.2912581939511,25.2452581744318,4.45096290982296));
#43855=CARTESIAN_POINT('Ctrl Pts',(-26.2962849266399,25.2370942645456,4.45155012616894));
#43856=CARTESIAN_POINT('Ctrl Pts',(-26.2980493786227,25.2342185152141,4.45175694080576));
#43857=CARTESIAN_POINT('Ctrl Pts',(-26.3015534850439,25.2284872610834,4.45216905063818));
#43858=CARTESIAN_POINT('Ctrl Pts',(-26.3032932179168,25.2256318089625,4.4523743426137));
#43859=CARTESIAN_POINT('Ctrl Pts',(-26.3071391088407,25.2192973192572,4.45282969238268));
#43860=CARTESIAN_POINT('Ctrl Pts',(-26.3092431290675,25.2158169962243,4.45307982817002));
#43861=CARTESIAN_POINT('Ctrl Pts',(-26.315292267501,25.20576802035,4.45380194020455));
#43862=CARTESIAN_POINT('Ctrl Pts',(-26.3192205345225,25.199189301694,4.45427453191398));
#43863=CARTESIAN_POINT('Ctrl Pts',(-26.3454841486131,25.1548467930436,4.45745901820239));
#43864=CARTESIAN_POINT('Ctrl Pts',(-26.3670688533068,25.1166458536685,4.46019805651753));
#43865=CARTESIAN_POINT('Ctrl Pts',(-26.4228465547749,25.0130464428213,4.46761920104715));
#43866=CARTESIAN_POINT('Ctrl Pts',(-26.4555827332692,24.9468976066703,4.47235083912952));
#43867=CARTESIAN_POINT('Ctrl Pts',(-26.5382496155191,24.7643459543721,4.48539226600775));
#43868=CARTESIAN_POINT('Ctrl Pts',(-26.5836337378715,24.6460365607246,4.49383098632803));
#43869=CARTESIAN_POINT('Ctrl Pts',(-26.6897355625017,24.3118101376062,4.51746475096486));
#43870=CARTESIAN_POINT('Ctrl Pts',(-26.7350780535578,24.0917502148828,4.53283010359708));
#43871=CARTESIAN_POINT('Ctrl Pts',(-26.7583603920194,23.8573250513762,4.54806094738001));
#43872=CARTESIAN_POINT('Ctrl Pts',(-26.7594347903948,23.8458854359024,4.5488012565424));
#43873=CARTESIAN_POINT('Ctrl Pts',(-26.7635206800514,23.7997310522971,4.55177564940515));
#43874=CARTESIAN_POINT('Ctrl Pts',(-26.7660303940838,23.7649726091436,4.55398723556093));
#43875=CARTESIAN_POINT('Ctrl Pts',(-26.7682332912513,23.7255769033781,4.55645661749159));
#43876=CARTESIAN_POINT('Ctrl Pts',(-26.7684807346502,23.720974640728,4.5567445189483));
#43877=CARTESIAN_POINT('Ctrl Pts',(-26.7688403924344,23.7140064781691,4.55717953579456));
#43878=CARTESIAN_POINT('Ctrl Pts',(-26.7689598715843,23.7116409839352,4.55732705700011));
#43879=CARTESIAN_POINT('Ctrl Pts',(-26.7691631738563,23.7075258872574,4.55758341839791));
#43880=CARTESIAN_POINT('Ctrl Pts',(-26.7692481783294,23.7057763484317,4.55769232538162));
#43881=CARTESIAN_POINT('Ctrl Pts',(-26.7694162766648,23.702257410642,4.55791120266558));
#43882=CARTESIAN_POINT('Ctrl Pts',(-26.7694993380181,23.7004880140099,4.55802117075398));
#43883=CARTESIAN_POINT('Ctrl Pts',(-26.7696672603877,23.6968467951451,4.55824729304731));
#43884=CARTESIAN_POINT('Ctrl Pts',(-26.7697519479626,23.6949749629049,4.55836343750543));
#43885=CARTESIAN_POINT('Ctrl Pts',(-26.7699454729076,23.690613274066,4.55863384858626));
#43886=CARTESIAN_POINT('Ctrl Pts',(-26.7700530548423,23.6881233586781,4.55878804447662));
#43887=CARTESIAN_POINT('Ctrl Pts',(-26.770325804334,23.6816362671151,4.55918933826552));
#43888=CARTESIAN_POINT('Ctrl Pts',(-26.7704864181719,23.6776388884537,4.55943618248145));
#43889=CARTESIAN_POINT('Ctrl Pts',(-26.7722005009939,23.6329021196836,4.56219398104913));
#43890=CARTESIAN_POINT('Ctrl Pts',(-26.7729883030933,23.5921350688961,4.5646628544902));
#43891=CARTESIAN_POINT('Ctrl Pts',(-26.7730023406925,23.55136208175,4.56709764253913));
#43892=CARTESIAN_POINT('Ctrl Pts',(-26.7730023395649,23.5513653520337,4.56709744725173));
#43893=CARTESIAN_POINT('Ctrl Pts',(-26.7731080939755,23.2450984785382,4.58538640618436));
#43894=CARTESIAN_POINT('Ctrl Pts',(-26.7295574972271,22.9403166062594,4.60176991163691));
#43895=CARTESIAN_POINT('Ctrl Pts',(-26.6111710850088,22.5352334404187,4.62578088064272));
#43896=CARTESIAN_POINT('Ctrl Pts',(-26.5727909509155,22.4260889674261,4.63247252524186));
#43897=CARTESIAN_POINT('Ctrl Pts',(-26.5092566950496,22.2723694869662,4.64237579605295));
#43898=CARTESIAN_POINT('Ctrl Pts',(-26.4887774108651,22.2259558102615,4.64543073087777));
#43899=CARTESIAN_POINT('Ctrl Pts',(-26.4638280111813,22.1728423376459,4.64900895928721));
#43900=CARTESIAN_POINT('Ctrl Pts',(-26.460417211027,22.1656506196963,4.64949522900745));
#43901=CARTESIAN_POINT('Ctrl Pts',(-26.4551963705043,22.1547469207156,4.65023520066626));
#43902=CARTESIAN_POINT('Ctrl Pts',(-26.45340576234,22.1510256251301,4.65048822582143));
#43903=CARTESIAN_POINT('Ctrl Pts',(-26.4501641761494,22.1443218729311,4.65094491393233));
#43904=CARTESIAN_POINT('Ctrl Pts',(-26.448715735039,22.1413381902163,4.65114848813569));
#43905=CARTESIAN_POINT('Ctrl Pts',(-26.4455893655727,22.1349233228556,4.65158684577235));
#43906=CARTESIAN_POINT('Ctrl Pts',(-26.4439099395751,22.1314928774113,4.65182168133922));
#43907=CARTESIAN_POINT('Ctrl Pts',(-26.4393428262965,22.1222057988774,4.65245857665054));
#43908=CARTESIAN_POINT('Ctrl Pts',(-26.4364434425008,22.1163549667174,4.65286104571327));
#43909=CARTESIAN_POINT('Ctrl Pts',(-26.4233445728212,22.0901227023089,4.65467107329236));
#43910=CARTESIAN_POINT('Ctrl Pts',(-26.4129470376788,22.069841400333,4.65608558051448));
#43911=CARTESIAN_POINT('Ctrl Pts',(-26.3965802747969,22.0387338524839,4.65827900850527));
#43912=CARTESIAN_POINT('Ctrl Pts',(-26.390762257781,22.0278285342838,4.65905252718635));
#43913=CARTESIAN_POINT('Ctrl Pts',(-26.3823708290075,22.012315158303,4.66015949216328));
#43914=CARTESIAN_POINT('Ctrl Pts',(-26.3798485564664,22.007679437637,4.66049112151599));
#43915=CARTESIAN_POINT('Ctrl Pts',(-26.3760552053937,22.0007481926207,4.66098823812281));
#43916=CARTESIAN_POINT('Ctrl Pts',(-26.374792682584,21.9984479745928,4.66115342236388));
#43917=CARTESIAN_POINT('Ctrl Pts',(-26.371696657672,21.9928235546415,4.66155784054046));
#43918=CARTESIAN_POINT('Ctrl Pts',(-26.3698600916257,21.9895010516831,4.66179718254879));
#43919=CARTESIAN_POINT('Ctrl Pts',(-26.3669776229357,21.9843081152788,4.66217195582481));
#43920=CARTESIAN_POINT('Ctrl Pts',(-26.3659357137498,21.9824354590785,4.66230724606277));
#43921=CARTESIAN_POINT('Ctrl Pts',(-26.3615216328583,21.9745204845051,4.66287966126024));
#43922=CARTESIAN_POINT('Ctrl Pts',(-26.3581318924703,21.9684880303125,4.66331740444321));
#43923=CARTESIAN_POINT('Ctrl Pts',(-26.3522294726293,21.9580627203142,4.66407647487299));
#43924=CARTESIAN_POINT('Ctrl Pts',(-26.3497258156795,21.953664762487,4.6643974843391));
#43925=CARTESIAN_POINT('Ctrl Pts',(-26.3452201086667,21.9457931583913,4.66497346186582));
#43926=CARTESIAN_POINT('Ctrl Pts',(-26.3432219115545,21.9423173091683,4.66522829475053));
#43927=CARTESIAN_POINT('Ctrl Pts',(-26.3390286260118,21.935054519799,4.6657618154092));
#43928=CARTESIAN_POINT('Ctrl Pts',(-26.3368322994535,21.931268307101,4.66604054593631));
#43929=CARTESIAN_POINT('Ctrl Pts',(-26.3243242217837,21.9098066857557,4.66762388829351));
#43930=CARTESIAN_POINT('Ctrl Pts',(-26.31385220005,21.8922256446288,4.6689340419198));
#43931=CARTESIAN_POINT('Ctrl Pts',(-26.14638626599,21.6170687594737,4.68964669635293));
#43932=CARTESIAN_POINT('Ctrl Pts',(-25.9541689463484,21.3827115993336,4.71037918464374));
#43933=CARTESIAN_POINT('Ctrl Pts',(-25.66786394157,21.1193073126764,4.73640666193883));
#43934=CARTESIAN_POINT('Ctrl Pts',(-25.6010836461156,21.0627101714906,4.74218758161736));
#43935=CARTESIAN_POINT('Ctrl Pts',(-25.5117208714353,20.993022406343,4.74947688656816));
#43936=CARTESIAN_POINT('Ctrl Pts',(-25.4911734836251,20.9773922718907,4.75112382488224));
#43937=CARTESIAN_POINT('Ctrl Pts',(-25.4626944688942,20.9562640183415,4.75336437592355));
#43938=CARTESIAN_POINT('Ctrl Pts',(-25.4549232929053,20.9505525744963,4.7539715209549));
#43939=CARTESIAN_POINT('Ctrl Pts',(-25.4433530546489,20.9421287311777,4.75486905867905));
#43940=CARTESIAN_POINT('Ctrl Pts',(-25.4395736358068,20.9393896254826,4.75516122945051));
#43941=CARTESIAN_POINT('Ctrl Pts',(-25.4335425840016,20.9350386190035,4.755625840048));
#43942=CARTESIAN_POINT('Ctrl Pts',(-25.4312948192377,20.9334214055301,4.75579864153974));
#43943=CARTESIAN_POINT('Ctrl Pts',(-25.4270215100568,20.9303552118266,4.75612647664754));
#43944=CARTESIAN_POINT('Ctrl Pts',(-25.4249963667343,20.9289056798118,4.75628154828341));
#43945=CARTESIAN_POINT('Ctrl Pts',(-25.4214559371121,20.9263777562859,4.75655213912213));
#43946=CARTESIAN_POINT('Ctrl Pts',(-25.419941395863,20.9252983277611,4.75666773064404));
#43947=CARTESIAN_POINT('Ctrl Pts',(-25.4169780645063,20.9231901980558,4.75689357568873));
#43948=CARTESIAN_POINT('Ctrl Pts',(-25.4155293615218,20.922161386429,4.75700383701278));
#43949=CARTESIAN_POINT('Ctrl Pts',(-25.4120681777767,20.9197076940537,4.75726691534394));
#43950=CARTESIAN_POINT('Ctrl Pts',(-25.4100549074439,20.9182839213028,4.75741965531588));
#43951=CARTESIAN_POINT('Ctrl Pts',(-25.4039605118889,20.9139844854646,4.75788116134603));
#43952=CARTESIAN_POINT('Ctrl Pts',(-25.3998743122096,20.9111159764467,4.75818943628167));
#43953=CARTESIAN_POINT('Ctrl Pts',(-25.357929543276,20.8818160473244,4.76134220996294));
#43954=CARTESIAN_POINT('Ctrl Pts',(-25.3195113750106,20.8561899606431,4.76413273441913));
#43955=CARTESIAN_POINT('Ctrl Pts',(-25.2090689588493,20.7859035529035,4.77192339098277));
#43956=CARTESIAN_POINT('Ctrl Pts',(-25.1358125902185,20.7432436811638,4.77682029692784));
#43957=CARTESIAN_POINT('Ctrl Pts',(-24.9951903290177,20.6686184002414,4.78588314065134));
#43958=CARTESIAN_POINT('Ctrl Pts',(-24.9282344309275,20.6360069997931,4.7900628209124));
#43959=CARTESIAN_POINT('Ctrl Pts',(-24.7263158052043,20.5461773337232,4.80242896775722));
#43960=CARTESIAN_POINT('Ctrl Pts',(-24.5885191558077,20.4958142286339,4.81056923182446));
#43961=CARTESIAN_POINT('Ctrl Pts',(-24.3542327213456,20.4278784264899,4.8244684736137));
#43962=CARTESIAN_POINT('Ctrl Pts',(-24.2595119543009,20.405009627322,4.83010105944297));
#43963=CARTESIAN_POINT('Ctrl Pts',(-24.1016884949517,20.3743978996075,4.83961505520899));
#43964=CARTESIAN_POINT('Ctrl Pts',(-24.0391317555486,20.3641686469608,4.84341839936489));
#43965=CARTESIAN_POINT('Ctrl Pts',(-23.9679985557683,20.3546811816255,4.84779283323655));
#43966=CARTESIAN_POINT('Ctrl Pts',(-23.9596756331334,20.3536041750684,4.84830542146305));
#43967=CARTESIAN_POINT('Ctrl Pts',(-23.9471621466664,20.3520345712205,4.84907726673279));
#43968=CARTESIAN_POINT('Ctrl Pts',(-23.9429746217936,20.3515176685281,4.84933575453622));
#43969=CARTESIAN_POINT('Ctrl Pts',(-23.935768917811,20.3506425685504,4.84978089139864));
#43970=CARTESIAN_POINT('Ctrl Pts',(-23.9327512174803,20.3502804137718,4.84996741506352));
#43971=CARTESIAN_POINT('Ctrl Pts',(-23.9265335168224,20.3495431472815,4.85035194503044));
#43972=CARTESIAN_POINT('Ctrl Pts',(-23.9233334579622,20.3491685644162,4.85054996784787));
#43973=CARTESIAN_POINT('Ctrl Pts',(-23.9156251172295,20.3482779803983,4.85102725207107));
#43974=CARTESIAN_POINT('Ctrl Pts',(-23.9111163055631,20.3477667019381,4.85130666243616));
#43975=CARTESIAN_POINT('Ctrl Pts',(-23.897265466571,20.3462257029244,4.85216572454044));
#43976=CARTESIAN_POINT('Ctrl Pts',(-23.8879200652376,20.3452273320687,4.85274636510446));
#43977=CARTESIAN_POINT('Ctrl Pts',(-23.7781856945582,20.3339896647524,4.85957647946691));
#43978=CARTESIAN_POINT('Ctrl Pts',(-23.6773837479637,20.3284309457564,4.8659730539542));
#43979=CARTESIAN_POINT('Ctrl Pts',(-23.2865409035751,20.3252481940312,4.89128583744409));
#43980=CARTESIAN_POINT('Ctrl Pts',(-22.9976137569462,20.3620338597635,4.91123962004421));
#43981=CARTESIAN_POINT('Ctrl Pts',(-22.6750831048697,20.4482965495018,4.93353845746264));
#43982=CARTESIAN_POINT('Ctrl Pts',(-22.6328249774174,20.4605309573818,4.93645679553918));
#43983=CARTESIAN_POINT('Ctrl Pts',(-22.5421524571281,20.4888065279282,4.94269421232781));
#43984=CARTESIAN_POINT('Ctrl Pts',(-22.4938398361696,20.5051400135801,4.94600239013901));
#43985=CARTESIAN_POINT('Ctrl Pts',(-22.4298143891178,20.5284930636405,4.95034771735269));
#43986=CARTESIAN_POINT('Ctrl Pts',(-22.4137432030588,20.5345008029068,4.95143512783788));
#43987=CARTESIAN_POINT('Ctrl Pts',(-22.3910540597094,20.5431896088852,4.95296483807384));
#43988=CARTESIAN_POINT('Ctrl Pts',(-22.384396183095,20.5457646392437,4.95341304185703));
#43989=CARTESIAN_POINT('Ctrl Pts',(-22.3742568684834,20.5497249446349,4.95409452629995));
#43990=CARTESIAN_POINT('Ctrl Pts',(-22.3707692521755,20.5510941840463,4.95432873954651));
#43991=CARTESIAN_POINT('Ctrl Pts',(-22.3643266818265,20.5536365154501,4.95476102024104));
#43992=CARTESIAN_POINT('Ctrl Pts',(-22.3613710660457,20.5548079017534,4.95495918885448));
#43993=CARTESIAN_POINT('Ctrl Pts',(-22.3565532056387,20.5567255974054,4.9552819735852));
#43994=CARTESIAN_POINT('Ctrl Pts',(-22.354689925029,20.5574692717613,4.95540674918188));
#43995=CARTESIAN_POINT('Ctrl Pts',(-22.351120013348,20.5588979643192,4.95564569428684));
#43996=CARTESIAN_POINT('Ctrl Pts',(-22.3494132791473,20.5595827013943,4.95575988015435));
#43997=CARTESIAN_POINT('Ctrl Pts',(-22.34545084411,20.5611763582942,4.95602486242271));
#43998=CARTESIAN_POINT('Ctrl Pts',(-22.3431955797708,20.5620863730443,4.95617559198756));
#43999=CARTESIAN_POINT('Ctrl Pts',(-22.3360980435863,20.5649596242419,4.95664968170279));
#44000=CARTESIAN_POINT('Ctrl Pts',(-22.331259483577,20.5669320973745,4.95697248265833));
#44001=CARTESIAN_POINT('Ctrl Pts',(-22.2918400988987,20.5831136004245,4.95959924185949));
#44002=CARTESIAN_POINT('Ctrl Pts',(-22.2575023223602,20.5979123614598,4.9618680555572));
#44003=CARTESIAN_POINT('Ctrl Pts',(-22.0646899096642,20.6850192365989,4.97454020938047));
#44004=CARTESIAN_POINT('Ctrl Pts',(-21.9120063636021,20.7694931697069,4.98432301941116));
#44005=CARTESIAN_POINT('Ctrl Pts',(-21.623098008461,20.9614317679698,5.00372174403504));
#44006=CARTESIAN_POINT('Ctrl Pts',(-21.4872224752447,21.0683539438096,5.0133128744892));
#44007=CARTESIAN_POINT('Ctrl Pts',(-21.2767831364495,21.2632250525258,5.02983228810096));
#44008=CARTESIAN_POINT('Ctrl Pts',(-21.1971875618686,21.3452040824698,5.03654678529588));
#44009=CARTESIAN_POINT('Ctrl Pts',(-21.1094023215744,21.4457949653686,5.04462759438187));
#44010=CARTESIAN_POINT('Ctrl Pts',(-21.0968208691804,21.4604763597784,5.0458031857543));
#44011=CARTESIAN_POINT('Ctrl Pts',(-21.0805866437075,21.4797688832802,5.04734342835977));
#44012=CARTESIAN_POINT('Ctrl Pts',(-21.0768131326725,21.4842782638783,5.04770311781997));
#44013=CARTESIAN_POINT('Ctrl Pts',(-21.0707018240331,21.491622076798,5.04828838332878));
#44014=CARTESIAN_POINT('Ctrl Pts',(-21.0683564837876,21.4944502384527,5.04851365112855));
#44015=CARTESIAN_POINT('Ctrl Pts',(-21.0638649131082,21.4998853511227,5.04894633494477));
#44016=CARTESIAN_POINT('Ctrl Pts',(-21.0617179324301,21.5024916781888,5.04915372003635));
#44017=CARTESIAN_POINT('Ctrl Pts',(-21.0568312514065,21.5084428990832,5.04962702840954));
#44018=CARTESIAN_POINT('Ctrl Pts',(-21.054094182448,21.5117899364984,5.0498930579097));
#44019=CARTESIAN_POINT('Ctrl Pts',(-21.0455866227044,21.5222362729809,5.05072284955111));
#44020=CARTESIAN_POINT('Ctrl Pts',(-21.0398396588414,21.5293545960459,5.05128756042851));
#44021=CARTESIAN_POINT('Ctrl Pts',(-20.9954431332286,21.584826779587,5.05568284231832));
#44022=CARTESIAN_POINT('Ctrl Pts',(-20.9581659837523,21.6342577724026,5.05956789186746));
#44023=CARTESIAN_POINT('Ctrl Pts',(-20.9194046445899,21.6888598748334,5.06383027233894));
#44024=CARTESIAN_POINT('Ctrl Pts',(-20.9164818231186,21.6929978151084,5.06415311152768));
#44025=CARTESIAN_POINT('Ctrl Pts',(-20.9008336227863,21.7152627412434,5.0658892492892));
#44026=CARTESIAN_POINT('Ctrl Pts',(-20.8882858447087,21.7335133084198,5.06730897193122));
#44027=CARTESIAN_POINT('Ctrl Pts',(-20.7103412717672,21.998132931136,5.08784568417336));
#44028=CARTESIAN_POINT('Ctrl Pts',(-20.5795754002199,22.2660443288315,5.10823386816402));
#44029=CARTESIAN_POINT('Ctrl Pts',(-20.4611676440061,22.6278950444826,5.1337139353049));
#44030=CARTESIAN_POINT('Ctrl Pts',(-20.4381513622476,22.7088149110581,5.13927558526879));
#44031=CARTESIAN_POINT('Ctrl Pts',(-20.4115050827481,22.8186658094726,5.14656730794082));
#44032=CARTESIAN_POINT('Ctrl Pts',(-20.405063342118,22.8468751255382,5.14841718946176));
#44033=CARTESIAN_POINT('Ctrl Pts',(-20.3968057065185,22.8854212543739,5.15091072586148));
#44034=CARTESIAN_POINT('Ctrl Pts',(-20.3946592931156,22.8956848681297,5.15157138793824));
#44035=CARTESIAN_POINT('Ctrl Pts',(-20.3915706368785,22.9108224042298,5.1525407578416));
#44036=CARTESIAN_POINT('Ctrl Pts',(-20.3905895268467,22.915688195226,5.15285158767963));
#44037=CARTESIAN_POINT('Ctrl Pts',(-20.3890549132902,22.9233908772446,5.15334241168979));
#44038=CARTESIAN_POINT('Ctrl Pts',(-20.388493982717,22.9262262545653,5.15352282221953));
#44039=CARTESIAN_POINT('Ctrl Pts',(-20.3874403241289,22.9315901534241,5.15386361612869));
#44040=CARTESIAN_POINT('Ctrl Pts',(-20.3869468124292,22.9341185160872,5.15402404402772));
#44041=CARTESIAN_POINT('Ctrl Pts',(-20.3860992079426,22.9384888318793,5.15430097852323));
#44042=CARTESIAN_POINT('Ctrl Pts',(-20.3857436911656,22.94033050479,5.154417567304));
#44043=CARTESIAN_POINT('Ctrl Pts',(-20.3850587304492,22.9438955069804,5.15464303343514));
#44044=CARTESIAN_POINT('Ctrl Pts',(-20.3847290864774,22.9456187924116,5.15475192231905));
#44045=CARTESIAN_POINT('Ctrl Pts',(-20.3839555910239,22.9496803789674,5.15500832922945));
#44046=CARTESIAN_POINT('Ctrl Pts',(-20.3835129214843,22.9520189081473,5.15515577905227));
#44047=CARTESIAN_POINT('Ctrl Pts',(-20.3822123550806,22.9589314183775,5.15559110042031));
#44048=CARTESIAN_POINT('Ctrl Pts',(-20.3813617698474,22.9635067947545,5.15587855475575));
#44049=CARTESIAN_POINT('Ctrl Pts',(-20.3740154361849,23.0035053600588,5.15838567186896));
#44050=CARTESIAN_POINT('Ctrl Pts',(-20.3681036458881,23.0390350721437,5.16057262237117));
#44051=CARTESIAN_POINT('Ctrl Pts',(-20.3619885068992,23.0800191322005,5.16305707973498));
#44052=CARTESIAN_POINT('Ctrl Pts',(-20.3612021363979,23.0853820993563,5.16338143277636));
#44053=CARTESIAN_POINT('Ctrl Pts',(-20.3602251032093,23.092164528227,5.16379071545343));
#44054=CARTESIAN_POINT('Ctrl Pts',(-20.360021856503,23.0935821336061,5.16387620946447));
#44055=CARTESIAN_POINT('Ctrl Pts',(-20.3559557582731,23.1220775497949,5.1655937207561));
#44056=CARTESIAN_POINT('Ctrl Pts',(-20.3524367177889,23.1492041508971,5.16721037273258));
#44057=CARTESIAN_POINT('Ctrl Pts',(-20.3328646643503,23.3167713462156,5.17710172693337));
#44058=CARTESIAN_POINT('Ctrl Pts',(-20.3257193454751,23.4581085851828,5.18503840838501));
#44059=CARTESIAN_POINT('Ctrl Pts',(-20.3308891944683,23.7966018910143,5.20397176602783));
#44060=CARTESIAN_POINT('Ctrl Pts',(-20.3519825270502,23.9930287674631,5.2149198754163));
#44061=CARTESIAN_POINT('Ctrl Pts',(-20.4029031128772,24.2459639053567,5.22992161685348));
#44062=CARTESIAN_POINT('Ctrl Pts',(-20.4166038651409,24.3052810330548,5.23350382593977));
#44063=CARTESIAN_POINT('Ctrl Pts',(-20.4433079402257,24.4075893087749,5.23981747159835));
#44064=CARTESIAN_POINT('Ctrl Pts',(-20.4555455899988,24.4507633201496,5.24252433699204));
#44065=CARTESIAN_POINT('Ctrl Pts',(-20.4709368775036,24.5010375198655,5.24573099980447));
#44066=CARTESIAN_POINT('Ctrl Pts',(-20.4732200156543,24.5084006859377,5.246202030221));
#44067=CARTESIAN_POINT('Ctrl Pts',(-20.476750912479,24.519645114573,5.24692348929501));
#44068=CARTESIAN_POINT('Ctrl Pts',(-20.4779796647221,24.5235323546042,5.24717329217977));
#44069=CARTESIAN_POINT('Ctrl Pts',(-20.4802297731954,24.5306040035871,5.24762845018184));
#44070=CARTESIAN_POINT('Ctrl Pts',(-20.481248717791,24.5337891788284,5.24783372555891));
#44071=CARTESIAN_POINT('Ctrl Pts',(-20.4833037806345,24.5401789247733,5.24824606178775));
#44072=CARTESIAN_POINT('Ctrl Pts',(-20.4843399681574,24.5433834686564,5.24845312471185));
#44073=CARTESIAN_POINT('Ctrl Pts',(-20.4872929233129,24.5524671987314,5.2490408452112));
#44074=CARTESIAN_POINT('Ctrl Pts',(-20.4892215840276,24.5583424770729,5.24942189537926));
#44075=CARTESIAN_POINT('Ctrl Pts',(-20.4974008851893,24.5830191808296,5.25102623102812));
#44076=CARTESIAN_POINT('Ctrl Pts',(-20.5038078272097,24.6017679911236,5.25225468225557));
#44077=CARTESIAN_POINT('Ctrl Pts',(-20.6392167035227,24.9863908158483,5.27765614416623));
#44078=CARTESIAN_POINT('Ctrl Pts',(-20.8330568032805,25.3260032904005,5.3044047976759));
#44079=CARTESIAN_POINT('Ctrl Pts',(-21.1198820019696,25.6675175975626,5.33410447590601));
#44080=CARTESIAN_POINT('Ctrl Pts',(-21.158558640892,25.7111119345917,5.33794637780967));
#44081=CARTESIAN_POINT('Ctrl Pts',(-21.2306153204169,25.7880240276761,5.3447836342117));
#44082=CARTESIAN_POINT('Ctrl Pts',(-21.2635850591232,25.8217037204597,5.34779951131197));
#44083=CARTESIAN_POINT('Ctrl Pts',(-21.301480142212,25.8587530723669,5.3511297741486));
#44084=CARTESIAN_POINT('Ctrl Pts',(-21.3056878527189,25.86284445617,5.35149771469782));
#44085=CARTESIAN_POINT('Ctrl Pts',(-21.3122458929754,25.8691864324528,5.35206829478371));
#44086=CARTESIAN_POINT('Ctrl Pts',(-21.3145884680548,25.8714449721888,5.35227154100182));
#44087=CARTESIAN_POINT('Ctrl Pts',(-21.3189786433865,25.8756648472263,5.35265137103907));
#44088=CARTESIAN_POINT('Ctrl Pts',(-21.3210254163184,25.8776270331644,5.35282802072079));
#44089=CARTESIAN_POINT('Ctrl Pts',(-21.3244688321559,25.8809194331155,5.35312447814667));
#44090=CARTESIAN_POINT('Ctrl Pts',(-21.3258640794771,25.8822510943442,5.35324439936297));
#44091=CARTESIAN_POINT('Ctrl Pts',(-21.3286413582422,25.8848970429266,5.35348270451323));
#44092=CARTESIAN_POINT('Ctrl Pts',(-21.3300233609256,25.8862113560606,5.35360109037877));
#44093=CARTESIAN_POINT('Ctrl Pts',(-21.3330722594389,25.8891057716524,5.35386183452936));
#44094=CARTESIAN_POINT('Ctrl Pts',(-21.3347396823231,25.8906853233141,5.35400414966931));
#44095=CARTESIAN_POINT('Ctrl Pts',(-21.3405662374345,25.8961930194413,5.35450046340097));
#44096=CARTESIAN_POINT('Ctrl Pts',(-21.3447341712098,25.9001119006454,5.35485374501852));
#44097=CARTESIAN_POINT('Ctrl Pts',(-21.3868050166998,25.939458287707,5.35840245567413));
#44098=CARTESIAN_POINT('Ctrl Pts',(-21.4255504040901,25.9739791909452,5.36152979959702));
#44099=CARTESIAN_POINT('Ctrl Pts',(-21.467671404388,26.0097208990934,5.36480424831003));
#44100=CARTESIAN_POINT('Ctrl Pts',(-21.4702310623164,26.0118860318649,5.36500275237122));
#44101=CARTESIAN_POINT('Ctrl Pts',(-21.4801647289094,26.0202620462487,5.36577127554351));
#44102=CARTESIAN_POINT('Ctrl Pts',(-21.4875632817881,26.0264438763656,5.36633974168597));
#44103=CARTESIAN_POINT('Ctrl Pts',(-21.6566820039388,26.1664663787064,5.37924774818872));
#44104=CARTESIAN_POINT('Ctrl Pts',(-21.8310838676421,26.2842351874449,5.39079777184254));
#44105=CARTESIAN_POINT('Ctrl Pts',(-22.0353830798098,26.3948594036574,5.40381141616256));
#44106=CARTESIAN_POINT('Ctrl Pts',(-22.0551571698946,26.4053019781705,5.40506566112819));
#44107=CARTESIAN_POINT('Ctrl Pts',(-22.0750360281848,26.4155367811664,5.40632238256859));
#44108=CARTESIAN_POINT('Origin',(-23.5502525316942,23.5502525316942,-77.3107734492734));
#44109=CARTESIAN_POINT('',(-22.0750360103879,26.4155367720035,6.90165778540197));
#44110=CARTESIAN_POINT('',(-22.0750360194354,26.4155367766617,6.65421995916068));
#44111=CARTESIAN_POINT('',(-22.0750360153461,26.4155367745563,-77.3107734492734));
#44112=CARTESIAN_POINT('',(-26.7730018951938,23.5482270531954,6.06297359389933));
#44113=CARTESIAN_POINT('Ctrl Pts',(-22.0750360103879,26.4155367720035,6.90165778540197));
#44114=CARTESIAN_POINT('Ctrl Pts',(-22.046006365424,26.4005906067135,6.89979682548396));
#44115=CARTESIAN_POINT('Ctrl Pts',(-22.0172022087877,26.3852024195089,6.89794726638968));
#44116=CARTESIAN_POINT('Ctrl Pts',(-21.6939193491592,26.2061239265263,6.87710186694981));
#44117=CARTESIAN_POINT('Ctrl Pts',(-21.4266592779431,25.997693552159,6.85877232401689));
#44118=CARTESIAN_POINT('Ctrl Pts',(-21.1830085908105,25.7371831942219,6.83719381506162));
#44119=CARTESIAN_POINT('Ctrl Pts',(-21.1696175015189,25.7225983660945,6.83599042232142));
#44120=CARTESIAN_POINT('Ctrl Pts',(-21.1522230852041,25.7032993384788,6.83440377706279));
#44121=CARTESIAN_POINT('Ctrl Pts',(-21.1480975297732,25.6986954851709,6.8340256985072));
#44122=CARTESIAN_POINT('Ctrl Pts',(-21.1417452057096,25.6915655313944,6.83344080788177));
#44123=CARTESIAN_POINT('Ctrl Pts',(-21.139509091468,25.6890477456583,6.83323438870156));
#44124=CARTESIAN_POINT('Ctrl Pts',(-21.135281077454,25.684272096585,6.83284308837805));
#44125=CARTESIAN_POINT('Ctrl Pts',(-21.1332883863516,25.6820149359416,6.83265824066074));
#44126=CARTESIAN_POINT('Ctrl Pts',(-21.1287509406063,25.6768607409035,6.83223636082794));
#44127=CARTESIAN_POINT('Ctrl Pts',(-21.1262082198912,25.673961929264,6.8319992441738));
#44128=CARTESIAN_POINT('Ctrl Pts',(-21.1192036793097,25.6659474807564,6.83134410469524));
#44129=CARTESIAN_POINT('Ctrl Pts',(-21.114752828987,25.660822321384,6.83092562641787));
#44130=CARTESIAN_POINT('Ctrl Pts',(-21.1048963070175,25.6493998287103,6.82999399663437));
#44131=CARTESIAN_POINT('Ctrl Pts',(-21.0994987157859,25.6430956151274,6.82948051413785));
#44132=CARTESIAN_POINT('Ctrl Pts',(-20.9698599840793,25.4904924924361,6.81706724212718));
#44133=CARTESIAN_POINT('Ctrl Pts',(-20.8589337269602,25.3334339159391,6.80461688179875));
#44134=CARTESIAN_POINT('Ctrl Pts',(-20.6109767273053,24.9060292105629,6.77161545760273));
#44135=CARTESIAN_POINT('Ctrl Pts',(-20.4968380000018,24.6245603924638,6.750593806451));
#44136=CARTESIAN_POINT('Ctrl Pts',(-20.4199247206499,24.3166683567566,6.73051498775437));
#44137=CARTESIAN_POINT('Ctrl Pts',(-20.4163691721878,24.3019975228268,6.72956528926706));
#44138=CARTESIAN_POINT('Ctrl Pts',(-20.4120045236128,24.2834188922671,6.72837198542093));
#44139=CARTESIAN_POINT('Ctrl Pts',(-20.4110994958829,24.2795341581376,6.72812298540666));
#44140=CARTESIAN_POINT('Ctrl Pts',(-20.4096564429428,24.2732875498949,6.72772343660979));
#44141=CARTESIAN_POINT('Ctrl Pts',(-20.4091138679424,24.2709267475513,6.72757262649262));
#44142=CARTESIAN_POINT('Ctrl Pts',(-20.4081544551746,24.2667305720654,6.7273049163297));
#44143=CARTESIAN_POINT('Ctrl Pts',(-20.40773656335,24.2648954450269,6.72718795509802));
#44144=CARTESIAN_POINT('Ctrl Pts',(-20.40686355856,24.261046165568,6.7269428694706));
#44145=CARTESIAN_POINT('Ctrl Pts',(-20.4064087747535,24.2590319461667,6.72681476450295));
#44146=CARTESIAN_POINT('Ctrl Pts',(-20.4052181371182,24.2537349674164,6.7264782434823));
#44147=CARTESIAN_POINT('Ctrl Pts',(-20.4044854846694,24.2504514795185,6.72627001292226));
#44148=CARTESIAN_POINT('Ctrl Pts',(-20.4012513024476,24.2358494879168,6.72534561955464));
#44149=CARTESIAN_POINT('Ctrl Pts',(-20.3988056664917,24.2245184982396,6.72463264692908));
#44150=CARTESIAN_POINT('Ctrl Pts',(-20.3810712965737,24.1401477477398,6.71935446354672));
#44151=CARTESIAN_POINT('Ctrl Pts',(-20.3682610296761,24.0666033327369,6.71492388573853));
#44152=CARTESIAN_POINT('Ctrl Pts',(-20.3467453892228,23.9113599333451,6.70580221882579));
#44153=CARTESIAN_POINT('Ctrl Pts',(-20.3385862151283,23.8296402424921,6.7011325309346));
#44154=CARTESIAN_POINT('Ctrl Pts',(-20.3134896637612,23.420770136293,6.67805133062961));
#44155=CARTESIAN_POINT('Ctrl Pts',(-20.343374228077,23.0927377950879,6.66019628025002));
#44156=CARTESIAN_POINT('Ctrl Pts',(-20.423322578879,22.7702209584271,6.64014345864616));
#44157=CARTESIAN_POINT('Ctrl Pts',(-20.424477195653,22.7656069216687,6.63985609567741));
#44158=CARTESIAN_POINT('Ctrl Pts',(-20.4305605808731,22.7415232479177,6.63835362648593));
#44159=CARTESIAN_POINT('Ctrl Pts',(-20.4356609703429,22.722097775616,6.63713310076293));
#44160=CARTESIAN_POINT('Ctrl Pts',(-20.4425773981241,22.6967236955165,6.63552704331468));
#44161=CARTESIAN_POINT('Ctrl Pts',(-20.4442296346503,22.6907305877161,6.6351468450622));
#44162=CARTESIAN_POINT('Ctrl Pts',(-20.4468054394549,22.6814918655835,6.6345594018824));
#44163=CARTESIAN_POINT('Ctrl Pts',(-20.4477167883685,22.6782428353272,6.63435255545733));
#44164=CARTESIAN_POINT('Ctrl Pts',(-20.4494522552211,22.6720929207778,6.63396053739416));
#44165=CARTESIAN_POINT('Ctrl Pts',(-20.4502753458729,22.6691917482577,6.6337753994562));
#44166=CARTESIAN_POINT('Ctrl Pts',(-20.4521580718491,22.6625909461244,6.63335369778098));
#44167=CARTESIAN_POINT('Ctrl Pts',(-20.453220262844,22.6588920557281,6.63311705077825));
#44168=CARTESIAN_POINT('Ctrl Pts',(-20.4561680777488,22.6486956964794,6.63246377200874));
#44169=CARTESIAN_POINT('Ctrl Pts',(-20.4580675326544,22.6422022765518,6.63204668838587));
#44170=CARTESIAN_POINT('Ctrl Pts',(-20.46233067982,22.6277969039272,6.63111904959555));
#44171=CARTESIAN_POINT('Ctrl Pts',(-20.4647043561962,22.6198879778117,6.63060816906519));
#44172=CARTESIAN_POINT('Ctrl Pts',(-20.4720239761866,22.5958356445136,6.62904962881855));
#44173=CARTESIAN_POINT('Ctrl Pts',(-20.4770663509738,22.5797221016729,6.62799880953517));
#44174=CARTESIAN_POINT('Ctrl Pts',(-20.495767156126,22.5215686434922,6.62418174911801));
#44175=CARTESIAN_POINT('Ctrl Pts',(-20.5101630248468,22.4797727655538,6.62139141257565));
#44176=CARTESIAN_POINT('Ctrl Pts',(-20.5619399498669,22.3389257912565,6.6118241455995));
#44177=CARTESIAN_POINT('Ctrl Pts',(-20.6033366474104,22.2414334087648,6.60491957556738));
#44178=CARTESIAN_POINT('Ctrl Pts',(-20.7764727540966,21.8837403012387,6.57855809952534));
#44179=CARTESIAN_POINT('Ctrl Pts',(-20.9385025931201,21.6397902497186,6.55831209814716));
#44180=CARTESIAN_POINT('Ctrl Pts',(-21.1342628928692,21.4173825559542,6.53911914339749));
#44181=CARTESIAN_POINT('Ctrl Pts',(-21.1374191502464,21.4138126560536,6.53881089888965));
#44182=CARTESIAN_POINT('Ctrl Pts',(-21.1438745704015,21.40654377433,6.53818292836507));
#44183=CARTESIAN_POINT('Ctrl Pts',(-21.1471743745237,21.4028453741799,6.53786323908622));
#44184=CARTESIAN_POINT('Ctrl Pts',(-21.1769136767446,21.3696681403749,6.53499390903361));
#44185=CARTESIAN_POINT('Ctrl Pts',(-21.2038873820847,21.3406696413679,6.53247532233303));
#44186=CARTESIAN_POINT('Ctrl Pts',(-21.2350786635353,21.3083525045086,6.5296637444229));
#44187=CARTESIAN_POINT('Ctrl Pts',(-21.2387765880974,21.3045400089444,6.52933198245303));
#44188=CARTESIAN_POINT('Ctrl Pts',(-21.2441928024521,21.2989835381699,6.52884837246776));
#44189=CARTESIAN_POINT('Ctrl Pts',(-21.2459036566359,21.2972323768466,6.52869594652076));
#44190=CARTESIAN_POINT('Ctrl Pts',(-21.2489359849817,21.2941356750015,6.52842638112218));
#44191=CARTESIAN_POINT('Ctrl Pts',(-21.2502566455962,21.2927893441246,6.52830917750864));
#44192=CARTESIAN_POINT('Ctrl Pts',(-21.253016950354,21.2899803227989,6.52806462797385));
#44193=CARTESIAN_POINT('Ctrl Pts',(-21.2544568070134,21.2885178511726,6.52793729970334));
#44194=CARTESIAN_POINT('Ctrl Pts',(-21.2582210786203,21.2847017547258,6.5276050331568));
#44195=CARTESIAN_POINT('Ctrl Pts',(-21.2605477295864,21.282350323851,6.5274002719067));
#44196=CARTESIAN_POINT('Ctrl Pts',(-21.2706752821995,21.2721463792809,6.52651159652928));
#44197=CARTESIAN_POINT('Ctrl Pts',(-21.2785131105357,21.2643303788513,6.52583057634219));
#44198=CARTESIAN_POINT('Ctrl Pts',(-21.3356143589554,21.2079719031026,6.52091627001857));
#44199=CARTESIAN_POINT('Ctrl Pts',(-21.3863929366002,21.1609819193639,6.51679873201299));
#44200=CARTESIAN_POINT('Ctrl Pts',(-21.5615722752598,21.0090430687963,6.5032565669248));
#44201=CARTESIAN_POINT('Ctrl Pts',(-21.6924042783877,20.9118812162692,6.49419719150604));
#44202=CARTESIAN_POINT('Ctrl Pts',(-22.0040525793919,20.7151624564374,6.47360437978621));
#44203=CARTESIAN_POINT('Ctrl Pts',(-22.1881820698076,20.622245964243,6.46207669216467));
#44204=CARTESIAN_POINT('Ctrl Pts',(-22.3845953787916,20.5456916108724,6.44962619723221));
#44205=CARTESIAN_POINT('Ctrl Pts',(-22.3892919458963,20.5438737393855,6.44932842394971));
#44206=CARTESIAN_POINT('Ctrl Pts',(-22.3977050305282,20.5406399923075,6.44879489216104));
#44207=CARTESIAN_POINT('Ctrl Pts',(-22.4014199522392,20.5392199706179,6.44855926062721));
#44208=CARTESIAN_POINT('Ctrl Pts',(-22.4161209425321,20.5336317121309,6.44762661789192));
#44209=CARTESIAN_POINT('Ctrl Pts',(-22.4271270498774,20.5295167310265,6.44692797859766));
#44210=CARTESIAN_POINT('Ctrl Pts',(-22.4398224756366,20.524849119214,6.44612154417997));
#44211=CARTESIAN_POINT('Ctrl Pts',(-22.4414901432593,20.5242375476571,6.44601560006298));
#44212=CARTESIAN_POINT('Ctrl Pts',(-22.4548568348715,20.5193482117978,6.44516634533394));
#44213=CARTESIAN_POINT('Ctrl Pts',(-22.4665799446985,20.5151369742952,6.44442095495116));
#44214=CARTESIAN_POINT('Ctrl Pts',(-22.4892224478524,20.50715112033,6.44298001722597));
#44215=CARTESIAN_POINT('Ctrl Pts',(-22.5001383171428,20.5033670448694,6.44228478536496));
#44216=CARTESIAN_POINT('Ctrl Pts',(-22.515501609529,20.4981336008166,6.4413054133809));
#44217=CARTESIAN_POINT('Ctrl Pts',(-22.5199322875163,20.4966350649463,6.4410228657423));
#44218=CARTESIAN_POINT('Ctrl Pts',(-22.5436532586617,20.4886697054947,6.43950958875571));
#44219=CARTESIAN_POINT('Ctrl Pts',(-22.5630008658028,20.4823761298768,6.43827328081423));
#44220=CARTESIAN_POINT('Ctrl Pts',(-22.5883664207331,20.4743897722676,6.43664936089408));
#44221=CARTESIAN_POINT('Ctrl Pts',(-22.5943318245346,20.4725306134498,6.43626723148297));
#44222=CARTESIAN_POINT('Ctrl Pts',(-22.6035331807905,20.4696922801963,6.43567746280351));
#44223=CARTESIAN_POINT('Ctrl Pts',(-22.6067653534869,20.4687008224243,6.43547022718088));
#44224=CARTESIAN_POINT('Ctrl Pts',(-22.6128877026517,20.4668333483331,6.43507755475712));
#44225=CARTESIAN_POINT('Ctrl Pts',(-22.6157775639809,20.4659563044061,6.43489215190516));
#44226=CARTESIAN_POINT('Ctrl Pts',(-22.6223462617721,20.4639728498192,6.43447060327651));
#44227=CARTESIAN_POINT('Ctrl Pts',(-22.6260258473688,20.4628689539228,6.43423437537795));
#44228=CARTESIAN_POINT('Ctrl Pts',(-22.6357165598435,20.4599805635921,6.43361199655701));
#44229=CARTESIAN_POINT('Ctrl Pts',(-22.6417309145564,20.4582070354329,6.43322548726326));
#44230=CARTESIAN_POINT('Ctrl Pts',(-22.6552732148509,20.4542565701417,6.43235463894453));
#44231=CARTESIAN_POINT('Ctrl Pts',(-22.6628039818134,20.4520895209574,6.43186997880298));
#44232=CARTESIAN_POINT('Ctrl Pts',(-22.6854719037923,20.4456560419578,6.43040992685186));
#44233=CARTESIAN_POINT('Ctrl Pts',(-22.7006322903253,20.4414729753752,6.42943182560527));
#44234=CARTESIAN_POINT('Ctrl Pts',(-22.7546296289051,20.4269984643464,6.4259420439738));
#44235=CARTESIAN_POINT('Ctrl Pts',(-22.7936264280118,20.4173228361798,6.42341060107046));
#44236=CARTESIAN_POINT('Ctrl Pts',(-22.9077547074845,20.3912611645688,6.41596715302887));
#44237=CARTESIAN_POINT('Ctrl Pts',(-22.9833001333683,20.3768327116259,6.41099570278561));
#44238=CARTESIAN_POINT('Ctrl Pts',(-23.4107164266459,20.310949195724,6.38263305986548));
#44239=CARTESIAN_POINT('Ctrl Pts',(-23.7686284494603,20.3153150366037,6.35764705120673));
#44240=CARTESIAN_POINT('Ctrl Pts',(-24.1339161056737,20.380757715556,6.33404670373366));
#44241=CARTESIAN_POINT('Ctrl Pts',(-24.1492403069917,20.3836180051432,6.33306084782847));
#44242=CARTESIAN_POINT('Ctrl Pts',(-24.1732676732397,20.3882834178933,6.33152233916795));
#44243=CARTESIAN_POINT('Ctrl Pts',(-24.181984922879,20.39001350061,6.33096566342429));
#44244=CARTESIAN_POINT('Ctrl Pts',(-24.1937862844089,20.3924064587527,6.33021418092985));
#44245=CARTESIAN_POINT('Ctrl Pts',(-24.196876636973,20.3930378133149,6.33001759395106));
#44246=CARTESIAN_POINT('Ctrl Pts',(-24.2017452986749,20.3940399221212,6.32970820275201));
#44247=CARTESIAN_POINT('Ctrl Pts',(-24.2035242193302,20.3944076425355,6.32959522410017));
#44248=CARTESIAN_POINT('Ctrl Pts',(-24.2069586448425,20.3951206004879,6.32937723610095));
#44249=CARTESIAN_POINT('Ctrl Pts',(-24.2086141777296,20.3954656347064,6.32927221609421));
#44250=CARTESIAN_POINT('Ctrl Pts',(-24.2125621814721,20.3962916922006,6.32902191135627));
#44251=CARTESIAN_POINT('Ctrl Pts',(-24.2148543982613,20.3967739114579,6.3288766964779));
#44252=CARTESIAN_POINT('Ctrl Pts',(-24.221688765416,20.3982194567446,6.32844406036627));
#44253=CARTESIAN_POINT('Ctrl Pts',(-24.226229386799,20.3991901055379,6.32815705996215));
#44254=CARTESIAN_POINT('Ctrl Pts',(-24.2640042596012,20.4073506495708,6.3257729118487));
#44255=CARTESIAN_POINT('Ctrl Pts',(-24.2971265048018,20.4150566424196,6.32370497009363));
#44256=CARTESIAN_POINT('Ctrl Pts',(-24.4166090202242,20.4448557399992,6.31630673124075));
#44257=CARTESIAN_POINT('Ctrl Pts',(-24.5021715100984,20.470006467984,6.31112547956491));
#44258=CARTESIAN_POINT('Ctrl Pts',(-24.7080971166735,20.5399401213598,6.29870110993601));
#44259=CARTESIAN_POINT('Ctrl Pts',(-24.8270380848266,20.5884277238055,6.29156098297286));
#44260=CARTESIAN_POINT('Ctrl Pts',(-25.0033060885696,20.6728825366777,6.28063592505208));
#44261=CARTESIAN_POINT('Ctrl Pts',(-25.0629156682402,20.7037682609793,6.27687872971753));
#44262=CARTESIAN_POINT('Ctrl Pts',(-25.2079689090717,20.784769090454,6.26750180382441));
#44263=CARTESIAN_POINT('Ctrl Pts',(-25.2921455854084,20.8370019340267,6.26184941998072));
#44264=CARTESIAN_POINT('Ctrl Pts',(-25.4509608337096,20.9459891620317,6.25061248798056));
#44265=CARTESIAN_POINT('Ctrl Pts',(-25.5257906786898,21.0022874260732,6.24504671241347));
#44266=CARTESIAN_POINT('Ctrl Pts',(-25.6059718734445,21.0682693432697,6.23872563201846));
#44267=CARTESIAN_POINT('Ctrl Pts',(-25.613852930858,21.0748180347975,6.23810035590868));
#44268=CARTESIAN_POINT('Ctrl Pts',(-25.6248591313593,21.0840526213941,6.23722148706006));
#44269=CARTESIAN_POINT('Ctrl Pts',(-25.6280106164732,21.0867071430689,6.23696918037101));
#44270=CARTESIAN_POINT('Ctrl Pts',(-25.633773046982,21.0915798080311,6.23650663879889));
#44271=CARTESIAN_POINT('Ctrl Pts',(-25.6363855666468,21.093796087942,6.23629648074741));
#44272=CARTESIAN_POINT('Ctrl Pts',(-25.641391493376,21.0980565133499,6.23589291386902));
#44273=CARTESIAN_POINT('Ctrl Pts',(-25.6437854503558,21.1001000083162,6.23569953205845));
#44274=CARTESIAN_POINT('Ctrl Pts',(-25.6487794054461,21.1043755387444,6.2352953148756));
#44275=CARTESIAN_POINT('Ctrl Pts',(-25.6513788437711,21.1066082193906,6.23508445290831));
#44276=CARTESIAN_POINT('Ctrl Pts',(-25.6604857135541,21.114455464861,6.23434409883854));
#44277=CARTESIAN_POINT('Ctrl Pts',(-25.6669741978161,21.1200918747641,6.23381369958372));
#44278=CARTESIAN_POINT('Ctrl Pts',(-25.7279363085686,21.1734777585898,6.22880267010499));
#44279=CARTESIAN_POINT('Ctrl Pts',(-25.7808041410448,21.2230217530364,6.22424682819144));
#44280=CARTESIAN_POINT('Ctrl Pts',(-25.8863672380138,21.3288516101607,6.21469116878159));
#44281=CARTESIAN_POINT('Ctrl Pts',(-25.9388021965948,21.3853315238309,6.20968456413662));
#44282=CARTESIAN_POINT('Ctrl Pts',(-26.0984356979744,21.5701447927488,6.19359957542516));
#44283=CARTESIAN_POINT('Ctrl Pts',(-26.1976942936307,21.7049590923145,6.18227917186331));
#44284=CARTESIAN_POINT('Ctrl Pts',(-26.385149767485,22.0060262466604,6.15828133088249));
#44285=CARTESIAN_POINT('Ctrl Pts',(-26.4701908773643,22.1735698217201,6.14565133545971));
#44286=CARTESIAN_POINT('Ctrl Pts',(-26.5444987945367,22.3583043093952,6.13310229821836));
#44287=CARTESIAN_POINT('Ctrl Pts',(-26.5487559332182,22.3690545771117,6.13237685063465));
#44288=CARTESIAN_POINT('Ctrl Pts',(-26.5542286374427,22.383094696012,6.13143588523676));
#44289=CARTESIAN_POINT('Ctrl Pts',(-26.5554967496718,22.3863637707323,6.13121724944211));
#44290=CARTESIAN_POINT('Ctrl Pts',(-26.5574392526297,22.3913957026248,6.13088142325365));
#44291=CARTESIAN_POINT('Ctrl Pts',(-26.5581174291337,22.3931570802963,6.13076400419729));
#44292=CARTESIAN_POINT('Ctrl Pts',(-26.5594626013033,22.3966599705246,6.13053075725797));
#44293=CARTESIAN_POINT('Ctrl Pts',(-26.5601296289103,22.3984014562902,6.13041492819999));
#44294=CARTESIAN_POINT('Ctrl Pts',(-26.5616136323905,22.4022860061321,6.13015685235958));
#44295=CARTESIAN_POINT('Ctrl Pts',(-26.5624298304494,22.4044293588006,6.13001465321585));
#44296=CARTESIAN_POINT('Ctrl Pts',(-26.5648079855288,22.410694543972,6.12959956643231));
#44297=CARTESIAN_POINT('Ctrl Pts',(-26.5663637831,22.4148187329556,6.12932705002879));
#44298=CARTESIAN_POINT('Ctrl Pts',(-26.5775623326941,22.4446898619168,6.12735837866613));
#44299=CARTESIAN_POINT('Ctrl Pts',(-26.5868841043074,22.4705570828485,6.12568119690994));
#44300=CARTESIAN_POINT('Ctrl Pts',(-26.6153313660208,22.5527803750207,6.12042749104709));
#44301=CARTESIAN_POINT('Ctrl Pts',(-26.6332285367491,22.609551269335,6.1169142286083));
#44302=CARTESIAN_POINT('Ctrl Pts',(-26.7312643049135,22.9534719895913,6.09613034252577));
#44303=CARTESIAN_POINT('Ctrl Pts',(-26.7728145267785,23.2501041940918,6.0801402810687));
#44304=CARTESIAN_POINT('Ctrl Pts',(-26.7730018951938,23.5482270531954,6.06297359389933));
#44305=CARTESIAN_POINT('Ctrl Pts',(-26.7730018977802,23.5482311726679,6.06297335668936));
#44306=CARTESIAN_POINT('Ctrl Pts',(-26.7730788051402,23.6708482547567,6.0559127436403));
#44307=CARTESIAN_POINT('Ctrl Pts',(-26.7661579448812,23.7933597209949,6.04869386501434));
#44308=CARTESIAN_POINT('Ctrl Pts',(-26.7512603658681,23.9240797248258,6.0407013465646));
#44309=CARTESIAN_POINT('Ctrl Pts',(-26.7502081414363,23.9329822247001,6.0401556051449));
#44310=CARTESIAN_POINT('Ctrl Pts',(-26.7484845246578,23.9470609549099,6.03929025637791));
#44311=CARTESIAN_POINT('Ctrl Pts',(-26.7478376719193,23.9522401882923,6.03897142324126));
#44312=CARTESIAN_POINT('Ctrl Pts',(-26.7467162760709,23.9610450139207,6.03842855412925));
#44313=CARTESIAN_POINT('Ctrl Pts',(-26.7462481378307,23.9646714235785,6.0382047208235));
#44314=CARTESIAN_POINT('Ctrl Pts',(-26.745366876741,23.971407760695,6.03778847681095));
#44315=CARTESIAN_POINT('Ctrl Pts',(-26.7449553820585,23.974517899833,6.03759611783517));
#44316=CARTESIAN_POINT('Ctrl Pts',(-26.7440934146059,23.9809604197764,6.03719727766523));
#44317=CARTESIAN_POINT('Ctrl Pts',(-26.7436422664471,23.984292705011,6.03699077530287));
#44318=CARTESIAN_POINT('Ctrl Pts',(-26.7426037825683,23.9918739215338,6.03652048747307));
#44319=CARTESIAN_POINT('Ctrl Pts',(-26.7420131787647,23.996122392135,6.03625659872505));
#44320=CARTESIAN_POINT('Ctrl Pts',(-26.7401935549154,24.0090228426967,6.03545425576304));
#44321=CARTESIAN_POINT('Ctrl Pts',(-26.7389378311826,24.0176709612638,6.03491495551422));
#44322=CARTESIAN_POINT('Ctrl Pts',(-26.7298079334654,24.0787987764774,6.03109274104929));
#44323=CARTESIAN_POINT('Ctrl Pts',(-26.7206741577155,24.13107940475,6.02776999844887));
#44324=CARTESIAN_POINT('Ctrl Pts',(-26.7081839411293,24.193446072919,6.02373831377344));
#44325=CARTESIAN_POINT('Ctrl Pts',(-26.7060628935246,24.2037735138671,6.02306845820368));
#44326=CARTESIAN_POINT('Ctrl Pts',(-26.7015340952358,24.22528809917,6.02166829055093));
#44327=CARTESIAN_POINT('Ctrl Pts',(-26.6991173620891,24.236473184748,6.02093771102794));
#44328=CARTESIAN_POINT('Ctrl Pts',(-26.6878525796614,24.2872959023935,6.01760598638686));
#44329=CARTESIAN_POINT('Ctrl Pts',(-26.6783156105871,24.3267756404533,6.01498418704338));
#44330=CARTESIAN_POINT('Ctrl Pts',(-26.6632405694166,24.3843879054442,6.01110901577964));
#44331=CARTESIAN_POINT('Ctrl Pts',(-26.6582842970997,24.4026696060045,6.00987201017383));
#44332=CARTESIAN_POINT('Ctrl Pts',(-26.6333332557562,24.4915923868539,6.00381982056796));
#44333=CARTESIAN_POINT('Ctrl Pts',(-26.6110907155913,24.5615764395919,5.99894671390942));
#44334=CARTESIAN_POINT('Ctrl Pts',(-26.4874676544983,24.9089648013869,5.974255416881));
#44335=CARTESIAN_POINT('Ctrl Pts',(-26.3506847438287,25.1722644190277,5.95375494604774));
#44336=CARTESIAN_POINT('Ctrl Pts',(-26.1726660175558,25.4235448371405,5.93433269184722));
#44337=CARTESIAN_POINT('Ctrl Pts',(-26.1653164863685,25.4337909777991,5.93354126377052));
#44338=CARTESIAN_POINT('Ctrl Pts',(-26.1558694157481,25.4467994565751,5.93253742301117));
#44339=CARTESIAN_POINT('Ctrl Pts',(-26.1538274287666,25.4496017203235,5.93232123426044));
#44340=CARTESIAN_POINT('Ctrl Pts',(-26.1505485077167,25.4540862322637,5.93197536214675));
#44341=CARTESIAN_POINT('Ctrl Pts',(-26.1493144615574,25.4557705733665,5.93184547811886));
#44342=CARTESIAN_POINT('Ctrl Pts',(-26.14696839853,25.4589661796505,5.9315991007346));
#44343=CARTESIAN_POINT('Ctrl Pts',(-26.145856707072,25.4604776618163,5.93148258639653));
#44344=CARTESIAN_POINT('Ctrl Pts',(-26.1433087861723,25.4639355448314,5.93121607391791));
#44345=CARTESIAN_POINT('Ctrl Pts',(-26.1418716868908,25.465881297444,5.93106613783984));
#44346=CARTESIAN_POINT('Ctrl Pts',(-26.1374433668317,25.4718628929275,5.93060529527919));
#44347=CARTESIAN_POINT('Ctrl Pts',(-26.1344448810463,25.4758933861057,5.9302948958556));
#44348=CARTESIAN_POINT('Ctrl Pts',(-26.1118493414853,25.5061179455114,5.92796801147204));
#44349=CARTESIAN_POINT('Ctrl Pts',(-26.0918629922861,25.5320204799883,5.92597834542153));
#44350=CARTESIAN_POINT('Ctrl Pts',(-26.0667296507002,25.5635877626773,5.923552923011));
#44351=CARTESIAN_POINT('Ctrl Pts',(-26.0619532925958,25.5695432816245,5.92309531217441));
#44352=CARTESIAN_POINT('Ctrl Pts',(-26.0526432885964,25.5810675466576,5.92220963121138));
#44353=CARTESIAN_POINT('Ctrl Pts',(-26.0481121105289,25.5866382150697,5.92178142396375));
#44354=CARTESIAN_POINT('Ctrl Pts',(-26.0425885997663,25.5933826910343,5.92126282475652));
#44355=CARTESIAN_POINT('Ctrl Pts',(-26.0416140353925,25.5945709467474,5.92117145069227));
#44356=CARTESIAN_POINT('Ctrl Pts',(-25.849807248885,25.828094074253,5.9032127537389));
#44357=CARTESIAN_POINT('Ctrl Pts',(-25.6273811160765,26.0326105959562,5.8871072642681));
#44358=CARTESIAN_POINT('Ctrl Pts',(-25.2965594964805,26.2607419276318,5.8642336720173));
#44359=CARTESIAN_POINT('Ctrl Pts',(-25.2106731056661,26.3141884399565,5.85839115733837));
#44360=CARTESIAN_POINT('Ctrl Pts',(-25.0859532107066,26.3838873527244,5.84993457362148));
#44361=CARTESIAN_POINT('Ctrl Pts',(-25.0490931158048,26.4035557995752,5.84743889864058));
#44362=CARTESIAN_POINT('Ctrl Pts',(-24.9899479618824,26.4336531679362,5.84343431589864));
#44363=CARTESIAN_POINT('Ctrl Pts',(-24.9679071755853,26.4445533832869,5.84194198948813));
#44364=CARTESIAN_POINT('Ctrl Pts',(-24.9399831596205,26.4579676474108,5.84005059667114));
#44365=CARTESIAN_POINT('Ctrl Pts',(-24.9342138516625,26.4607180402109,5.83965978273793));
#44366=CARTESIAN_POINT('Ctrl Pts',(-24.9255442297187,26.464819488344,5.83907243034146));
#44367=CARTESIAN_POINT('Ctrl Pts',(-24.9226499989544,26.466183427856,5.83887633926477));
#44368=CARTESIAN_POINT('Ctrl Pts',(-24.9167272993387,26.4689637969299,5.83847503589178));
#44369=CARTESIAN_POINT('Ctrl Pts',(-24.9136986486562,26.4703798279657,5.83826981009486));
#44370=CARTESIAN_POINT('Ctrl Pts',(-24.9076074114677,26.4732162142819,5.83785702842776));
#44371=CARTESIAN_POINT('Ctrl Pts',(-24.9045447859199,26.4746364752587,5.83764946961424));
#44372=CARTESIAN_POINT('Ctrl Pts',(-24.8958293382696,26.4786615467764,5.83705876306828));
#44373=CARTESIAN_POINT('Ctrl Pts',(-24.8901712167838,26.4812547866381,5.83667521622037));
#44374=CARTESIAN_POINT('Ctrl Pts',(-24.8661685927903,26.492171682046,5.83504788219857));
#44375=CARTESIAN_POINT('Ctrl Pts',(-24.8477540863078,26.5003394885749,5.83379874376687));
#44376=CARTESIAN_POINT('Ctrl Pts',(-24.8110792609782,26.5161969093896,5.83130920106765));
#44377=CARTESIAN_POINT('Ctrl Pts',(-24.7928221909294,26.5238918350581,5.83006904572971));
#44378=CARTESIAN_POINT('Ctrl Pts',(-24.7671195747605,26.5344468523977,5.82832176093346));
#44379=CARTESIAN_POINT('Ctrl Pts',(-24.7597323330181,26.5374484999179,5.82781941280882));
#44380=CARTESIAN_POINT('Ctrl Pts',(-24.745911335889,26.5430046939857,5.82687924866301));
#44381=CARTESIAN_POINT('Ctrl Pts',(-24.7394803293032,26.5455659919426,5.82644166006604));
#44382=CARTESIAN_POINT('Ctrl Pts',(-24.7274897028574,26.5502968349387,5.82562553793013));
#44383=CARTESIAN_POINT('Ctrl Pts',(-24.7219322019276,26.552471698943,5.82524718128342));
#44384=CARTESIAN_POINT('Ctrl Pts',(-24.7125820818593,26.5561008442503,5.82461045959413));
#44385=CARTESIAN_POINT('Ctrl Pts',(-24.7087926806107,26.5575634209094,5.82435236543096));
#44386=CARTESIAN_POINT('Ctrl Pts',(-24.6918841220338,26.5640528329838,5.82320053090046));
#44387=CARTESIAN_POINT('Ctrl Pts',(-24.678735094805,26.5690009542944,5.82230426010669));
#44388=CARTESIAN_POINT('Ctrl Pts',(-24.6330457337568,26.5858541262252,5.81918803896817));
#44389=CARTESIAN_POINT('Ctrl Pts',(-24.6003469055514,26.5973199453145,5.81695443881186));
#44390=CARTESIAN_POINT('Ctrl Pts',(-24.4155799677924,26.6587810433475,5.80431500092033));
#44391=CARTESIAN_POINT('Ctrl Pts',(-24.2601522704044,26.6979140786884,5.79359712790687));
#44392=CARTESIAN_POINT('Ctrl Pts',(-24.0851301336834,26.7283547260324,5.78158687802584));
#44393=CARTESIAN_POINT('Ctrl Pts',(-24.0677580919096,26.7312296769987,5.78039561856338));
#44394=CARTESIAN_POINT('Ctrl Pts',(-24.030565466361,26.7370720555219,5.77784767530869));
#44395=CARTESIAN_POINT('Ctrl Pts',(-24.0107389562223,26.7399972620547,5.77649092698763));
#44396=CARTESIAN_POINT('Ctrl Pts',(-23.9679475341717,26.7459034303317,5.77356703035208));
#44397=CARTESIAN_POINT('Ctrl Pts',(-23.9449750815039,26.7488221957486,5.77200004290516));
#44398=CARTESIAN_POINT('Ctrl Pts',(-23.894740328477,26.7546553378737,5.76858126917683));
#44399=CARTESIAN_POINT('Ctrl Pts',(-23.8674680785046,26.7574699405713,5.7667302389359));
#44400=CARTESIAN_POINT('Ctrl Pts',(-23.7457701323822,26.7684621488717,5.75849976883083));
#44401=CARTESIAN_POINT('Ctrl Pts',(-23.6510402228595,26.7728205441744,5.75217070720347));
#44402=CARTESIAN_POINT('Ctrl Pts',(-23.514829734828,26.7730740352416,5.74329381802271));
#44403=CARTESIAN_POINT('Ctrl Pts',(-23.473409436445,26.7723525801453,5.74062435334669));
#44404=CARTESIAN_POINT('Ctrl Pts',(-23.4112938818087,26.7700720753166,5.73667713749036));
#44405=CARTESIAN_POINT('Ctrl Pts',(-23.3905824827673,26.7691114800839,5.73537036818875));
#44406=CARTESIAN_POINT('Ctrl Pts',(-23.3658110665697,26.7677228930343,5.73381980122999));
#44407=CARTESIAN_POINT('Ctrl Pts',(-23.3617413896576,26.7674870164535,5.73356545950237));
#44408=CARTESIAN_POINT('Ctrl Pts',(-23.3554533756924,26.7671105938254,5.73317310806402));
#44409=CARTESIAN_POINT('Ctrl Pts',(-23.3532347367553,26.7669754746327,5.73303479334844));
#44410=CARTESIAN_POINT('Ctrl Pts',(-23.3493404521675,26.7667342614434,5.73279222994697));
#44411=CARTESIAN_POINT('Ctrl Pts',(-23.3476647564267,26.7666291537423,5.7326879257588));
#44412=CARTESIAN_POINT('Ctrl Pts',(-23.3441130437561,26.7664035865907,5.73246699653627));
#44413=CARTESIAN_POINT('Ctrl Pts',(-23.3422370554818,26.7662827955598,5.73235039081233));
#44414=CARTESIAN_POINT('Ctrl Pts',(-23.3368995816647,26.7659344368019,5.73201887579972));
#44415=CARTESIAN_POINT('Ctrl Pts',(-23.333438342883,26.7657029206635,5.7318041898975));
#44416=CARTESIAN_POINT('Ctrl Pts',(-23.3187531401536,26.7646968337508,5.73089455385596));
#44417=CARTESIAN_POINT('Ctrl Pts',(-23.3075327229963,26.763869068029,5.73020257061449));
#44418=CARTESIAN_POINT('Ctrl Pts',(-23.2909229678065,26.7625562243158,5.72918241102737));
#44419=CARTESIAN_POINT('Ctrl Pts',(-23.28553029882,26.7621163172079,5.72885185221613));
#44420=CARTESIAN_POINT('Ctrl Pts',(-22.9952102458591,26.7376973084817,5.71108992595839));
#44421=CARTESIAN_POINT('Ctrl Pts',(-22.7146851389304,26.6759147574256,5.69561502083473));
#44422=CARTESIAN_POINT('Ctrl Pts',(-22.3206690118792,26.532202931748,5.67203495157881));
#44423=CARTESIAN_POINT('Ctrl Pts',(-22.1983456332645,26.478775513242,5.66444346522528));
#44424=CARTESIAN_POINT('Ctrl Pts',(-22.0781380349912,26.4171322838288,5.65650890082168));
#44425=CARTESIAN_POINT('Ctrl Pts',(-22.0765866962736,26.4163351561205,5.65640642003244));
#44426=CARTESIAN_POINT('Ctrl Pts',(-22.0750360153137,26.4155367745396,5.65630390104212));
#44427=CARTESIAN_POINT('Ctrl Pts',(-22.0750360281848,26.4155367811664,5.40632238256859));
#44428=CARTESIAN_POINT('Ctrl Pts',(-22.1527963909306,26.4555723798902,5.41123831454265));
#44429=CARTESIAN_POINT('Ctrl Pts',(-22.2321597963147,26.4924287425938,5.41619338139705));
#44430=CARTESIAN_POINT('Ctrl Pts',(-22.3901205810958,26.5581088994348,5.42605094954073));
#44431=CARTESIAN_POINT('Ctrl Pts',(-22.4685253872204,26.5871869715262,5.43094162592195));
#44432=CARTESIAN_POINT('Ctrl Pts',(-22.5910746905245,26.627288871437,5.43863918610307));
#44433=CARTESIAN_POINT('Ctrl Pts',(-22.6344730309378,26.6404826775678,5.44137490383914));
#44434=CARTESIAN_POINT('Ctrl Pts',(-22.685576553372,26.6548479623116,5.44461241544078));
#44435=CARTESIAN_POINT('Ctrl Pts',(-22.6930268245531,26.6569133468898,5.44508479890216));
#44436=CARTESIAN_POINT('Ctrl Pts',(-22.7044215157217,26.6600281046258,5.44580790328134));
#44437=CARTESIAN_POINT('Ctrl Pts',(-22.7083606532161,26.6610968361063,5.44605799397193));
#44438=CARTESIAN_POINT('Ctrl Pts',(-22.7155312108755,26.6630276704382,5.44651345461904));
#44439=CARTESIAN_POINT('Ctrl Pts',(-22.7187619676795,26.6638922330135,5.44671874429687));
#44440=CARTESIAN_POINT('Ctrl Pts',(-22.7252461255434,26.665616606121,5.44713092120141));
#44441=CARTESIAN_POINT('Ctrl Pts',(-22.7284995390503,26.6664763531428,5.44733781020008));
#44442=CARTESIAN_POINT('Ctrl Pts',(-22.7377218001677,26.6688979811658,5.44792449637284));
#44443=CARTESIAN_POINT('Ctrl Pts',(-22.7436937710024,26.6704478130651,5.44830468390117));
#44444=CARTESIAN_POINT('Ctrl Pts',(-22.7687529812387,26.6768743701678,5.44990117477486));
#44445=CARTESIAN_POINT('Ctrl Pts',(-22.7878799616148,26.6815930920325,5.45112258144023));
#44446=CARTESIAN_POINT('Ctrl Pts',(-22.8117416350575,26.6872483045731,5.4526501137397));
#44447=CARTESIAN_POINT('Ctrl Pts',(-22.8164370732838,26.6883499960985,5.45295087890532));
#44448=CARTESIAN_POINT('Ctrl Pts',(-22.8327017304964,26.6921276753268,5.45399334323447));
#44449=CARTESIAN_POINT('Ctrl Pts',(-22.8442831475457,26.694750232922,5.45473675354819));
#44450=CARTESIAN_POINT('Ctrl Pts',(-22.8674822425642,26.6998689357183,5.45622818715308));
#44451=CARTESIAN_POINT('Ctrl Pts',(-22.879099758761,26.7023649518838,5.45697620163019));
#44452=CARTESIAN_POINT('Ctrl Pts',(-22.8923346813743,26.7051319826366,5.45782968213867));
#44453=CARTESIAN_POINT('Ctrl Pts',(-22.8939389266158,26.705466106006,5.45793315724208));
#44454=CARTESIAN_POINT('Ctrl Pts',(-22.9023922451765,26.7072199906981,5.45847851994595));
#44455=CARTESIAN_POINT('Ctrl Pts',(-22.9092456311313,26.7086186663045,5.45892106781193));
#44456=CARTESIAN_POINT('Ctrl Pts',(-22.9194457635329,26.7106657965379,5.45958033363931));
#44457=CARTESIAN_POINT('Ctrl Pts',(-22.9227891057499,26.7113312767301,5.45979652087203));
#44458=CARTESIAN_POINT('Ctrl Pts',(-22.9301837741407,26.7127909650504,5.4602748897395));
#44459=CARTESIAN_POINT('Ctrl Pts',(-22.9342355784513,26.7135826946103,5.46053714761841));
#44460=CARTESIAN_POINT('Ctrl Pts',(-22.9441705717884,26.7155041976366,5.46118055226377));
#44461=CARTESIAN_POINT('Ctrl Pts',(-22.9500553943893,26.7166253534695,5.46156196280872));
#44462=CARTESIAN_POINT('Ctrl Pts',(-22.9763409666862,26.7215572775595,5.46326694734642));
#44463=CARTESIAN_POINT('Ctrl Pts',(-22.9967747673052,26.7251872725367,5.46459599173609));
#44464=CARTESIAN_POINT('Ctrl Pts',(-23.3158327622133,26.7786931515335,5.48540477581826));
#44465=CARTESIAN_POINT('Ctrl Pts',(-23.6199644741039,26.7864322828912,5.50622337556283));
#44466=CARTESIAN_POINT('Ctrl Pts',(-23.9883285605163,26.743816873924,5.53101933811224));
#44467=CARTESIAN_POINT('Ctrl Pts',(-24.0557790674879,26.7338366531908,5.53553233446592));
#44468=CARTESIAN_POINT('Ctrl Pts',(-24.1721153258687,26.7128319837487,5.54321597682523));
#44469=CARTESIAN_POINT('Ctrl Pts',(-24.2211542572648,26.7027933607203,5.5464234193737));
#44470=CARTESIAN_POINT('Ctrl Pts',(-24.2758636829127,26.6902593658756,5.54995150318833));
#44471=CARTESIAN_POINT('Ctrl Pts',(-24.2817809423806,26.6888860954037,5.55033242920677));
#44472=CARTESIAN_POINT('Ctrl Pts',(-24.2909409929071,26.6867329300221,5.55092104367419));
#44473=CARTESIAN_POINT('Ctrl Pts',(-24.2941864768339,26.6859647269023,5.55112938691081));
#44474=CARTESIAN_POINT('Ctrl Pts',(-24.2995835408699,26.6846783959997,5.55147549772328));
#44475=CARTESIAN_POINT('Ctrl Pts',(-24.3017357805697,26.6841630899055,5.55161342630976));
#44476=CARTESIAN_POINT('Ctrl Pts',(-24.3059210532599,26.6831564597769,5.55188145998747));
#44477=CARTESIAN_POINT('Ctrl Pts',(-24.3079541413923,26.6826653729082,5.5520115787169));
#44478=CARTESIAN_POINT('Ctrl Pts',(-24.3117598374919,26.6817421955005,5.55225498514339));
#44479=CARTESIAN_POINT('Ctrl Pts',(-24.3135325446572,26.6813105818019,5.55236829941502));
#44480=CARTESIAN_POINT('Ctrl Pts',(-24.3175602344447,26.6803263075194,5.55262560813788));
#44481=CARTESIAN_POINT('Ctrl Pts',(-24.319814982708,26.6797727164655,5.55276954759721));
#44482=CARTESIAN_POINT('Ctrl Pts',(-24.3255398997912,26.6783605602793,5.55313475482223));
#44483=CARTESIAN_POINT('Ctrl Pts',(-24.3290092522136,26.6774986544286,5.55335582897626));
#44484=CARTESIAN_POINT('Ctrl Pts',(-24.348063417831,26.6727312731513,5.55456868958115));
#44485=CARTESIAN_POINT('Ctrl Pts',(-24.3636206541268,26.6687149771228,5.5555541433478));
#44486=CARTESIAN_POINT('Ctrl Pts',(-24.6806651840772,26.5843319309292,5.57555061034941));
#44487=CARTESIAN_POINT('Ctrl Pts',(-24.9689874130604,26.4607057467485,5.59225749175479));
#44488=CARTESIAN_POINT('Ctrl Pts',(-25.3030797971255,26.2558169366057,5.61442016861978));
#44489=CARTESIAN_POINT('Ctrl Pts',(-25.3695126912894,26.2116006054066,5.61897627918916));
#44490=CARTESIAN_POINT('Ctrl Pts',(-25.5116683487789,26.1091731238215,5.6291510190953));
#44491=CARTESIAN_POINT('Ctrl Pts',(-25.5865794939861,26.0499718022262,5.63479805206794));
#44492=CARTESIAN_POINT('Ctrl Pts',(-25.6718188270182,25.9762312392442,5.64162817813586));
#44493=CARTESIAN_POINT('Ctrl Pts',(-25.6847975151681,25.9648195591982,5.64267973781968));
#44494=CARTESIAN_POINT('Ctrl Pts',(-25.7018872896687,25.9495476809719,5.6440801244155));
#44495=CARTESIAN_POINT('Ctrl Pts',(-25.7060810972827,25.9457801437716,5.64442504913626));
#44496=CARTESIAN_POINT('Ctrl Pts',(-25.7129517103185,25.9395752246995,5.64499223415765));
#44497=CARTESIAN_POINT('Ctrl Pts',(-25.7156343447951,25.9371442912539,5.64521422125183));
#44498=CARTESIAN_POINT('Ctrl Pts',(-25.7208253997667,25.932424338826,5.64564480982305));
#44499=CARTESIAN_POINT('Ctrl Pts',(-25.7233343105921,25.9301358642101,5.64585338800971));
#44500=CARTESIAN_POINT('Ctrl Pts',(-25.7291195391586,25.9248421577146,5.64633542918354));
#44501=CARTESIAN_POINT('Ctrl Pts',(-25.7323932590183,25.9218341082076,5.64660901214717));
#44502=CARTESIAN_POINT('Ctrl Pts',(-25.7411556841848,25.9137492714149,5.64734346012603));
#44503=CARTESIAN_POINT('Ctrl Pts',(-25.7466329399245,25.908660164631,5.6478048524037));
#44504=CARTESIAN_POINT('Ctrl Pts',(-25.7850605141236,25.8727058106497,5.65105823434949));
#44505=CARTESIAN_POINT('Ctrl Pts',(-25.8173753456759,25.8411715095583,5.65387905699424));
#44506=CARTESIAN_POINT('Ctrl Pts',(-25.8538241279906,25.8040765109968,5.65716266604942));
#44507=CARTESIAN_POINT('Ctrl Pts',(-25.8586167535975,25.7991676583308,5.65759650997082));
#44508=CARTESIAN_POINT('Ctrl Pts',(-25.8677171125332,25.7897868658124,5.65842429464836));
#44509=CARTESIAN_POINT('Ctrl Pts',(-25.8720276727756,25.785317700886,5.65881811248597));
#44510=CARTESIAN_POINT('Ctrl Pts',(-25.8868340968147,25.7698774280966,5.66017680174864));
#44511=CARTESIAN_POINT('Ctrl Pts',(-25.8972652073454,25.758844748262,5.66114436789616));
#44512=CARTESIAN_POINT('Ctrl Pts',(-25.9095400846546,25.7456768078444,5.66229536958803));
#44513=CARTESIAN_POINT('Ctrl Pts',(-25.9114596287637,25.7436121817592,5.66247572671434));
#44514=CARTESIAN_POINT('Ctrl Pts',(-25.9399292869548,25.7129100596076,5.66515609662126));
#44515=CARTESIAN_POINT('Ctrl Pts',(-25.9659585242726,25.6837958129243,5.66767674708013));
#44516=CARTESIAN_POINT('Ctrl Pts',(-26.0037643115757,25.6399303097492,5.67144344623523));
#44517=CARTESIAN_POINT('Ctrl Pts',(-26.0159513176634,25.6255363064559,5.67267462499127));
#44518=CARTESIAN_POINT('Ctrl Pts',(-26.167243159694,25.443632386992,5.68817247413242));
#44519=CARTESIAN_POINT('Ctrl Pts',(-26.2891406853652,25.2625610524322,5.70301018125796));
#44520=CARTESIAN_POINT('Ctrl Pts',(-26.4299672463416,24.9993530736216,5.72313861301102));
#44521=CARTESIAN_POINT('Ctrl Pts',(-26.4654021567287,24.9266802334914,5.72855297554233));
#44522=CARTESIAN_POINT('Ctrl Pts',(-26.527387766687,24.7863940628209,5.73864900096001));
#44523=CARTESIAN_POINT('Ctrl Pts',(-26.5544605580201,24.7190622323026,5.74334598832455));
#44524=CARTESIAN_POINT('Ctrl Pts',(-26.5831311666554,24.6401583053523,5.74863486150997));
#44525=CARTESIAN_POINT('Ctrl Pts',(-26.5869659837205,24.6294276006317,5.74934959185833));
#44526=CARTESIAN_POINT('Ctrl Pts',(-26.591852313135,24.6155222208977,5.75026970386431));
#44527=CARTESIAN_POINT('Ctrl Pts',(-26.592955850827,24.6123661099792,5.75047813882302));
#44528=CARTESIAN_POINT('Ctrl Pts',(-26.5947314830746,24.6072623339677,5.75081454277809));
#44529=CARTESIAN_POINT('Ctrl Pts',(-26.5954066212884,24.6053157422107,5.75094269346581));
#44530=CARTESIAN_POINT('Ctrl Pts',(-26.5966954034865,24.6015883197709,5.75118778465723));
#44531=CARTESIAN_POINT('Ctrl Pts',(-26.5973093510205,24.5998076041877,5.75130474287788));
#44532=CARTESIAN_POINT('Ctrl Pts',(-26.598712389226,24.5957265742201,5.75157249039693));
#44533=CARTESIAN_POINT('Ctrl Pts',(-26.5995004393128,24.5934258991435,5.75172321723081));
#44534=CARTESIAN_POINT('Ctrl Pts',(-26.6019733991446,24.5861794639706,5.75219728985586));
#44535=CARTESIAN_POINT('Ctrl Pts',(-26.6036488969936,24.5812304650825,5.75252007651023));
#44536=CARTESIAN_POINT('Ctrl Pts',(-26.6172131458675,24.5408419771263,5.7551464674736));
#44537=CARTESIAN_POINT('Ctrl Pts',(-26.6284971395042,24.5052003253937,5.7574149381736));
#44538=CARTESIAN_POINT('Ctrl Pts',(-26.7276756842679,24.171887398887,5.77824357025283));
#44539=CARTESIAN_POINT('Ctrl Pts',(-26.7727688909504,23.8631384923526,5.79482711162516));
#44540=CARTESIAN_POINT('Ctrl Pts',(-26.7730558073513,23.4803904694763,5.81660196983098));
#44541=CARTESIAN_POINT('Ctrl Pts',(-26.7706784790624,23.4081346848806,5.820757844145));
#44542=CARTESIAN_POINT('Ctrl Pts',(-26.7639330475648,23.3068846978194,5.8266849154569));
#44543=CARTESIAN_POINT('Ctrl Pts',(-26.7615959060808,23.2777749763216,5.8284009460084));
#44544=CARTESIAN_POINT('Ctrl Pts',(-26.7578948780875,23.2383946924825,5.83074071663151));
#44545=CARTESIAN_POINT('Ctrl Pts',(-26.7568765622641,23.2280925445392,5.83135451323139));
#44546=CARTESIAN_POINT('Ctrl Pts',(-26.7502995805126,23.1646771671542,5.83514359689672));
#44547=CARTESIAN_POINT('Ctrl Pts',(-26.7434713374447,23.111706501012,5.83835562339637));
#44548=CARTESIAN_POINT('Ctrl Pts',(-26.7339956421314,23.0502784946369,5.84214330286811));
#44549=CARTESIAN_POINT('Ctrl Pts',(-26.7326254973083,23.0416303375923,5.84267800323797));
#44550=CARTESIAN_POINT('Ctrl Pts',(-26.7305311035279,23.0287506646893,5.8434765296463));
#44551=CARTESIAN_POINT('Ctrl Pts',(-26.7298336073664,23.0245147884245,5.84373950447742));
#44552=CARTESIAN_POINT('Ctrl Pts',(-26.7285745700901,23.0169628408019,5.84420898790239));
#44553=CARTESIAN_POINT('Ctrl Pts',(-26.728016296591,23.0136462248568,5.84441539219418));
#44554=CARTESIAN_POINT('Ctrl Pts',(-26.7268284589082,23.0066563299915,5.84485086267765));
#44555=CARTESIAN_POINT('Ctrl Pts',(-26.7261977130818,23.0029832593101,5.84507996623825));
#44556=CARTESIAN_POINT('Ctrl Pts',(-26.7245151153017,22.9932857343654,5.84568555894803));
#44557=CARTESIAN_POINT('Ctrl Pts',(-26.7234524875928,22.9872631871438,5.84606239114273));
#44558=CARTESIAN_POINT('Ctrl Pts',(-26.7185702282646,22.9600454824409,5.84776876505117));
#44559=CARTESIAN_POINT('Ctrl Pts',(-26.7145554076472,22.9388863072757,5.84910452239508));
#44560=CARTESIAN_POINT('Ctrl Pts',(-26.6835971495884,22.784209527204,5.85893853321938));
#44561=CARTESIAN_POINT('Ctrl Pts',(-26.6484288569967,22.6524969504501,5.86770137465535));
#44562=CARTESIAN_POINT('Ctrl Pts',(-26.5511796703,22.3631850110311,5.88782992172599));
#44563=CARTESIAN_POINT('Ctrl Pts',(-26.4847991295889,22.2074491102723,5.8992892378728));
#44564=CARTESIAN_POINT('Ctrl Pts',(-26.3911234001205,22.0281896964588,5.91297077355295));
#44565=CARTESIAN_POINT('Ctrl Pts',(-26.37527267516,21.9989679695246,5.91521681489622));
#44566=CARTESIAN_POINT('Ctrl Pts',(-26.2848186485942,21.8381965332728,5.92764661797554));
#44567=CARTESIAN_POINT('Ctrl Pts',(-26.2014688471973,21.7117607734551,5.93770294965426));
#44568=CARTESIAN_POINT('Ctrl Pts',(-26.1038037485723,21.5841440177507,5.94780974515509));
#44569=CARTESIAN_POINT('Ctrl Pts',(-26.0980391603917,21.5766796787852,5.94840069764547));
#44570=CARTESIAN_POINT('Ctrl Pts',(-26.0902546704426,21.5666907988375,5.94919113042513));
#44571=CARTESIAN_POINT('Ctrl Pts',(-26.0882636916173,21.5641439331466,5.94939263308698));
#44572=CARTESIAN_POINT('Ctrl Pts',(-26.0851382107318,21.5601581836546,5.94970791797973));
#44573=CARTESIAN_POINT('Ctrl Pts',(-26.0840063149882,21.5587172732633,5.94982188620929));
#44574=CARTESIAN_POINT('Ctrl Pts',(-26.0818299870855,21.5559516528076,5.95004060718245));
#44575=CARTESIAN_POINT('Ctrl Pts',(-26.0807857505092,21.5546268060977,5.9501453725113));
#44576=CARTESIAN_POINT('Ctrl Pts',(-26.0783103137437,21.5514912302543,5.95039330005524));
#44577=CARTESIAN_POINT('Ctrl Pts',(-26.0768782097856,21.5496812201923,5.95053639623526));
#44578=CARTESIAN_POINT('Ctrl Pts',(-26.0726625460843,21.544364866753,5.95095664432539));
#44579=CARTESIAN_POINT('Ctrl Pts',(-26.0698736085411,21.5408627649384,5.95123341075544));
#44580=CARTESIAN_POINT('Ctrl Pts',(-26.0488276057264,21.5145477621958,5.95331263219949));
#44581=CARTESIAN_POINT('Ctrl Pts',(-26.0302675854028,21.491977334311,5.9550936148071));
#44582=CARTESIAN_POINT('Ctrl Pts',(-25.9666352924829,21.4167061224595,5.96103713860791));
#44583=CARTESIAN_POINT('Ctrl Pts',(-25.9201673205921,21.3652053340056,5.96511065761663));
#44584=CARTESIAN_POINT('Ctrl Pts',(-25.7596399773988,21.1984432560415,5.97848242196879));
#44585=CARTESIAN_POINT('Ctrl Pts',(-25.6385497292089,21.0902888794698,5.98747023165775));
#44586=CARTESIAN_POINT('Ctrl Pts',(-25.3162684750233,20.8434560493402,6.01017310538728));
#44587=CARTESIAN_POINT('Ctrl Pts',(-25.1065466313101,20.7176771584164,6.02396960561583));
#44588=CARTESIAN_POINT('Ctrl Pts',(-24.8707975533494,20.6104378088753,6.03968099973521));
#44589=CARTESIAN_POINT('Ctrl Pts',(-24.8568828061011,20.6042268915719,6.04060871319477));
#44590=CARTESIAN_POINT('Ctrl Pts',(-24.837833003299,20.5958854272061,6.04187947151056));
#44591=CARTESIAN_POINT('Ctrl Pts',(-24.8327355529198,20.5936690712461,6.04221957432103));
#44592=CARTESIAN_POINT('Ctrl Pts',(-24.8246555023374,20.5901807175809,6.04275879090372));
#44593=CARTESIAN_POINT('Ctrl Pts',(-24.8216766561265,20.5889000075966,6.04295760664374));
#44594=CARTESIAN_POINT('Ctrl Pts',(-24.8156605137503,20.5863242086915,6.04335919087196));
#44595=CARTESIAN_POINT('Ctrl Pts',(-24.8126231501236,20.5850292877295,6.0435619648091));
#44596=CARTESIAN_POINT('Ctrl Pts',(-24.8057050530171,20.5820924475287,6.04402387882783));
#44597=CARTESIAN_POINT('Ctrl Pts',(-24.8018230845308,20.5804534695467,6.04428311873339));
#44598=CARTESIAN_POINT('Ctrl Pts',(-24.7936930691182,20.5770397259692,6.04482614423634));
#44599=CARTESIAN_POINT('Ctrl Pts',(-24.7894444140477,20.5752664415432,6.0451099795932));
#44600=CARTESIAN_POINT('Ctrl Pts',(-24.7782843266129,20.5706365494942,6.04585569464476));
#44601=CARTESIAN_POINT('Ctrl Pts',(-24.7713667549985,20.5677948969837,6.04631808132575));
#44602=CARTESIAN_POINT('Ctrl Pts',(-24.7507690002305,20.5594172694581,6.04769537947554));
#44603=CARTESIAN_POINT('Ctrl Pts',(-24.7370607556829,20.5539512142618,6.04861265037018));
#44604=CARTESIAN_POINT('Ctrl Pts',(-24.5872650093573,20.4954105719419,6.05864393356026));
#44605=CARTESIAN_POINT('Ctrl Pts',(-24.4477769021305,20.451560295609,6.06806761322516));
#44606=CARTESIAN_POINT('Ctrl Pts',(-24.0095782453884,20.3458810971131,6.09789791554048));
#44607=CARTESIAN_POINT('Ctrl Pts',(-23.7047404822808,20.3168191900896,6.11910705652832));
#44608=CARTESIAN_POINT('Ctrl Pts',(-23.3973217112458,20.3311316797424,6.13898132329279));
#44609=CARTESIAN_POINT('Ctrl Pts',(-23.3942702431048,20.3312780954639,6.13917842830714));
#44610=CARTESIAN_POINT('Ctrl Pts',(-23.3850958304794,20.3317313789008,6.13977051907922));
#44611=CARTESIAN_POINT('Ctrl Pts',(-23.3789735116455,20.3320513811406,6.14016494427671));
#44612=CARTESIAN_POINT('Ctrl Pts',(-23.3376929327138,20.3343271744853,6.14281958040853));
#44613=CARTESIAN_POINT('Ctrl Pts',(-23.3025660670445,20.3368417027629,6.14505487186846));
#44614=CARTESIAN_POINT('Ctrl Pts',(-23.2628804181231,20.3403372362001,6.14754821341587));
#44615=CARTESIAN_POINT('Ctrl Pts',(-23.2582759539783,20.3407527864685,6.14783701028041));
#44616=CARTESIAN_POINT('Ctrl Pts',(-23.2513102548497,20.3413965509994,6.14827314970318));
#44617=CARTESIAN_POINT('Ctrl Pts',(-23.2489483761315,20.3416174643088,6.14842090102293));
#44618=CARTESIAN_POINT('Ctrl Pts',(-23.2448420039836,20.3420061191788,6.14867755056071));
#44619=CARTESIAN_POINT('Ctrl Pts',(-23.2430974037475,20.3421726758826,6.14878651593827));
#44620=CARTESIAN_POINT('Ctrl Pts',(-23.2394460844198,20.342524272532,6.14901441904033));
#44621=CARTESIAN_POINT('Ctrl Pts',(-23.237539395512,20.3427095893821,6.1491333404588));
#44622=CARTESIAN_POINT('Ctrl Pts',(-23.2329798252601,20.3431568520141,6.14941751632879));
#44623=CARTESIAN_POINT('Ctrl Pts',(-23.2303270935925,20.3434203903046,6.14958268023829));
#44624=CARTESIAN_POINT('Ctrl Pts',(-23.221338377157,20.3443246478362,6.1501417740387));
#44625=CARTESIAN_POINT('Ctrl Pts',(-23.2150039131638,20.3449808609985,6.1505348313706));
#44626=CARTESIAN_POINT('Ctrl Pts',(-23.1999547505997,20.3465849662621,6.1514664870729));
#44627=CARTESIAN_POINT('Ctrl Pts',(-23.1912418399859,20.3475496524718,6.15200416358644));
#44628=CARTESIAN_POINT('Ctrl Pts',(-23.0888365076416,20.3593110368342,6.15830456193933));
#44629=CARTESIAN_POINT('Ctrl Pts',(-22.9956475108253,20.3741811543608,6.16385052936836));
#44630=CARTESIAN_POINT('Ctrl Pts',(-22.5166689270653,20.472342077844,6.19199571541734));
#44631=CARTESIAN_POINT('Ctrl Pts',(-22.1479505743331,20.621870525189,6.21290550838715));
#44632=CARTESIAN_POINT('Ctrl Pts',(-21.7994448375427,20.8444907963224,6.23793649323792));
#44633=CARTESIAN_POINT('Ctrl Pts',(-21.7836209265199,20.8547958174311,6.23908457069594));
#44634=CARTESIAN_POINT('Ctrl Pts',(-21.7628342584268,20.8685944094484,6.2406083905364));
#44635=CARTESIAN_POINT('Ctrl Pts',(-21.7577892787743,20.8719639261937,6.24097945730516));
#44636=CARTESIAN_POINT('Ctrl Pts',(-21.7499780537418,20.8772129601438,6.24155591203842));
#44637=CARTESIAN_POINT('Ctrl Pts',(-21.7472051503858,20.8790825843372,6.24176092544901));
#44638=CARTESIAN_POINT('Ctrl Pts',(-21.7417186753603,20.8827942640434,6.24216731749311));
#44639=CARTESIAN_POINT('Ctrl Pts',(-21.7390049951073,20.8846361526466,6.24236868963623));
#44640=CARTESIAN_POINT('Ctrl Pts',(-21.7329877234052,20.888733758312,6.24281602358636));
#44641=CARTESIAN_POINT('Ctrl Pts',(-21.7296855147117,20.8909914875399,6.24306206173605));
#44642=CARTESIAN_POINT('Ctrl Pts',(-21.7228355616794,20.8956935586184,6.2435735727137));
#44643=CARTESIAN_POINT('Ctrl Pts',(-21.7192885000737,20.8981388768035,6.24383908250656));
#44644=CARTESIAN_POINT('Ctrl Pts',(-21.7101759274258,20.9044480118911,6.24452283894024));
#44645=CARTESIAN_POINT('Ctrl Pts',(-21.7046176990124,20.908322265799,6.24494148470431));
#44646=CARTESIAN_POINT('Ctrl Pts',(-21.6885168876838,20.9196206270153,6.24615884101707));
#44647=CARTESIAN_POINT('Ctrl Pts',(-21.6780066848585,20.9270904499103,6.24695930680067));
#44648=CARTESIAN_POINT('Ctrl Pts',(-21.5735151558612,21.0023026823741,6.25497620470894));
#44649=CARTESIAN_POINT('Ctrl Pts',(-21.483217321754,21.0749951593829,6.26238580172256));
#44650=CARTESIAN_POINT('Ctrl Pts',(-21.1566280115007,21.3682627506778,6.29110557425273));
#44651=CARTESIAN_POINT('Ctrl Pts',(-20.9500926625425,21.6190247166904,6.31362026413936));
#44652=CARTESIAN_POINT('Ctrl Pts',(-20.7823272901686,21.8995792651776,6.33491691902024));
#44653=CARTESIAN_POINT('Ctrl Pts',(-20.7803579426909,21.902886044983,6.33516740636562));
#44654=CARTESIAN_POINT('Ctrl Pts',(-20.7761215722387,21.9100285122519,6.3357072962221));
#44655=CARTESIAN_POINT('Ctrl Pts',(-20.7738565669367,21.9138653949012,6.33599660807987));
#44656=CARTESIAN_POINT('Ctrl Pts',(-20.768740919468,21.92257241645,6.33665150736507));
#44657=CARTESIAN_POINT('Ctrl Pts',(-20.7658950891353,21.9274453837391,6.33701687234371));
#44658=CARTESIAN_POINT('Ctrl Pts',(-20.7403143285272,21.9715131727814,6.3403103976156));
#44659=CARTESIAN_POINT('Ctrl Pts',(-20.7183940968227,22.0111784598735,6.3431994638552));
#44660=CARTESIAN_POINT('Ctrl Pts',(-20.6950063540492,22.0556918959894,6.34634793786345));
#44661=CARTESIAN_POINT('Ctrl Pts',(-20.6927064900214,22.0600938658941,6.34665828951856));
#44662=CARTESIAN_POINT('Ctrl Pts',(-20.6892829869668,22.0666835663226,6.34712136384703));
#44663=CARTESIAN_POINT('Ctrl Pts',(-20.6881516748567,22.0688672690902,6.3472745692147));
#44664=CARTESIAN_POINT('Ctrl Pts',(-20.6862080997611,22.0726293708434,6.34753808186566));
#44665=CARTESIAN_POINT('Ctrl Pts',(-20.685394641398,22.0742071455313,6.34764846522299));
#44666=CARTESIAN_POINT('Ctrl Pts',(-20.6837137232085,22.0774740596891,6.34787675235189));
#44667=CARTESIAN_POINT('Ctrl Pts',(-20.6828464541295,22.0791632908539,6.3479946434623));
#44668=CARTESIAN_POINT('Ctrl Pts',(-20.6808082753509,22.0831418221231,6.34827195374635));
#44669=CARTESIAN_POINT('Ctrl Pts',(-20.6796386084345,22.0854317651505,6.34843129368368));
#44670=CARTESIAN_POINT('Ctrl Pts',(-20.6758257718895,22.0929185417324,6.34895135902176));
#44671=CARTESIAN_POINT('Ctrl Pts',(-20.6731939443701,22.0981211870342,6.34931136942247));
#44672=CARTESIAN_POINT('Ctrl Pts',(-20.6187632505012,22.2064496453276,6.35677918888949));
#44673=CARTESIAN_POINT('Ctrl Pts',(-20.5725196660176,22.3122907233276,6.36354489169143));
#44674=CARTESIAN_POINT('Ctrl Pts',(-20.3987921155106,22.7763723759413,6.39192381602653));
#44675=CARTESIAN_POINT('Ctrl Pts',(-20.3295564568571,23.1530899055787,6.41218509498876));
#44676=CARTESIAN_POINT('Ctrl Pts',(-20.327435545196,23.5544120673456,6.43644400443614));
#44677=CARTESIAN_POINT('Ctrl Pts',(-20.3275325714907,23.5756031723385,6.43773132561476));
#44678=CARTESIAN_POINT('Ctrl Pts',(-20.3279302599021,23.6031396574205,6.43941287491131));
#44679=CARTESIAN_POINT('Ctrl Pts',(-20.328040701733,23.6094875998691,6.43980112439245));
#44680=CARTESIAN_POINT('Ctrl Pts',(-20.3282468041674,23.6196134411999,6.44042141415273));
#44681=CARTESIAN_POINT('Ctrl Pts',(-20.328330353619,23.6233915925089,6.44065307382721));
#44682=CARTESIAN_POINT('Ctrl Pts',(-20.3284991958094,23.6304639024051,6.44108712698656));
#44683=CARTESIAN_POINT('Ctrl Pts',(-20.3285828959775,23.633758097068,6.44128947017852));
#44684=CARTESIAN_POINT('Ctrl Pts',(-20.3287818555187,23.6411425105352,6.44174342767195));
#44685=CARTESIAN_POINT('Ctrl Pts',(-20.3288998525165,23.6452326444578,6.44199512765288));
#44686=CARTESIAN_POINT('Ctrl Pts',(-20.3292678196502,23.6571969694445,6.44273215481603));
#44687=CARTESIAN_POINT('Ctrl Pts',(-20.3295388725616,23.6650704401269,6.44321814347493));
#44688=CARTESIAN_POINT('Ctrl Pts',(-20.3302173455139,23.6828792196343,6.44431960564494));
#44689=CARTESIAN_POINT('Ctrl Pts',(-20.3306418827256,23.692813760903,6.44493561347629));
#44690=CARTESIAN_POINT('Ctrl Pts',(-20.3321390734126,23.7244194674938,6.44690043097967));
#44691=CARTESIAN_POINT('Ctrl Pts',(-20.333384592742,23.7460814827299,6.44825465081802));
#44692=CARTESIAN_POINT('Ctrl Pts',(-20.3390275281155,23.8295127085533,6.45350041325461));
#44693=CARTESIAN_POINT('Ctrl Pts',(-20.3449859587357,23.8911595863106,6.45744024440367));
#44694=CARTESIAN_POINT('Ctrl Pts',(-20.3736183205356,24.1187105038635,6.47222588172824));
#44695=CARTESIAN_POINT('Ctrl Pts',(-20.4074311517312,24.2829260760923,6.48339502353272));
#44696=CARTESIAN_POINT('Ctrl Pts',(-20.4933603184843,24.5807122107429,6.50432963492038));
#44697=CARTESIAN_POINT('Ctrl Pts',(-20.541924970244,24.7149001627361,6.51402983396284));
#44698=CARTESIAN_POINT('Ctrl Pts',(-20.642668495061,24.9444416631128,6.53072393770521));
#44699=CARTESIAN_POINT('Ctrl Pts',(-20.6910826124488,25.0412123988521,6.53779279858136));
#44700=CARTESIAN_POINT('Ctrl Pts',(-20.7475560566604,25.1411813446359,6.54499279424933));
#44701=CARTESIAN_POINT('Ctrl Pts',(-20.7508535721495,25.1469765172854,6.54540979239078));
#44702=CARTESIAN_POINT('Ctrl Pts',(-20.7554217573912,25.1549471605623,6.5459827547767));
#44703=CARTESIAN_POINT('Ctrl Pts',(-20.7566769984934,25.1571313850362,6.54613970615585));
#44704=CARTESIAN_POINT('Ctrl Pts',(-20.7588290898082,25.1608660603782,6.54640796293511));
#44705=CARTESIAN_POINT('Ctrl Pts',(-20.7597246711814,25.1624172349514,6.54651935069508));
#44706=CARTESIAN_POINT('Ctrl Pts',(-20.7614731403522,25.1654398153731,6.54673633633047));
#44707=CARTESIAN_POINT('Ctrl Pts',(-20.7623258973667,25.1669112886831,6.5468419419993));
#44708=CARTESIAN_POINT('Ctrl Pts',(-20.7643889091324,25.1704646282566,6.54709689219001));
#44709=CARTESIAN_POINT('Ctrl Pts',(-20.7656003358622,25.1725458188956,6.54724615994889));
#44710=CARTESIAN_POINT('Ctrl Pts',(-20.7693182820324,25.1789166915076,6.54770292636924));
#44711=CARTESIAN_POINT('Ctrl Pts',(-20.7718324044901,25.1832019626115,6.54800993096234));
#44712=CARTESIAN_POINT('Ctrl Pts',(-20.7981838412058,25.2278804127643,6.55120853065695));
#44713=CARTESIAN_POINT('Ctrl Pts',(-20.8228918702673,25.2677570518982,6.55404417511084));
#44714=CARTESIAN_POINT('Ctrl Pts',(-20.8971079950609,25.381892355827,6.56214701615865));
#44715=CARTESIAN_POINT('Ctrl Pts',(-20.9488428926592,25.4546555262145,6.56729628191907));
#44716=CARTESIAN_POINT('Ctrl Pts',(-21.0242540891823,25.5518999839783,6.5742908725811));
#44717=CARTESIAN_POINT('Ctrl Pts',(-21.045392429882,25.5782901538094,6.57620111199282));
#44718=CARTESIAN_POINT('Ctrl Pts',(-21.2476402070929,25.8227992959622,6.5940617134665));
#44719=CARTESIAN_POINT('Ctrl Pts',(-21.4563542578339,26.0164387658367,6.60956868193696));
#44720=CARTESIAN_POINT('Ctrl Pts',(-21.6910908424768,26.1826758605299,6.62661349338064));
#44721=CARTESIAN_POINT('Ctrl Pts',(-21.6944806058583,26.1850666291031,6.62685952638634));
#44722=CARTESIAN_POINT('Ctrl Pts',(-21.7007424301596,26.1894649569934,6.62731382846861));
#44723=CARTESIAN_POINT('Ctrl Pts',(-21.7036131708846,26.1914743914597,6.62752203097897));
#44724=CARTESIAN_POINT('Ctrl Pts',(-21.7121750511035,26.197446674774,6.62814277759251));
#44725=CARTESIAN_POINT('Ctrl Pts',(-21.7178756863467,26.2013958230617,6.62855580498542));
#44726=CARTESIAN_POINT('Ctrl Pts',(-21.7252110792776,26.2064424977994,6.6290869444804));
#44727=CARTESIAN_POINT('Ctrl Pts',(-21.7268341862455,26.2075569885702,6.62920444932175));
#44728=CARTESIAN_POINT('Ctrl Pts',(-21.7329337387332,26.2117369676924,6.6296459501258));
#44729=CARTESIAN_POINT('Ctrl Pts',(-21.7374168840679,26.2147926256837,6.6299702971106));
#44730=CARTESIAN_POINT('Ctrl Pts',(-21.7442329670014,26.2194132211194,6.63046320589802));
#44731=CARTESIAN_POINT('Ctrl Pts',(-21.7465602844139,26.2209864628549,6.63063146802716));
#44732=CARTESIAN_POINT('Ctrl Pts',(-21.7637254476448,26.2325572596121,6.63187220768163));
#44733=CARTESIAN_POINT('Ctrl Pts',(-21.7786440363856,26.2424339883102,6.63294902149212));
#44734=CARTESIAN_POINT('Ctrl Pts',(-21.8114845262292,26.2637845852591,6.63531663869885));
#44735=CARTESIAN_POINT('Ctrl Pts',(-21.8294392805941,26.2752061282996,6.63660928716948));
#44736=CARTESIAN_POINT('Ctrl Pts',(-21.8529046291673,26.2898087183467,6.63829684299885));
#44737=CARTESIAN_POINT('Ctrl Pts',(-21.8583136605233,26.29315261324,6.63868571866198));
#44738=CARTESIAN_POINT('Ctrl Pts',(-21.8669547850541,26.2984593211348,6.6393067763534));
#44739=CARTESIAN_POINT('Ctrl Pts',(-21.8701805163449,26.3004325047901,6.63953857612161));
#44740=CARTESIAN_POINT('Ctrl Pts',(-21.8762248421344,26.304115223277,6.63997284555408));
#44741=CARTESIAN_POINT('Ctrl Pts',(-21.8790426039066,26.3058261211017,6.64017526479139));
#44742=CARTESIAN_POINT('Ctrl Pts',(-21.885361828606,26.3096497907629,6.64062915410262));
#44743=CARTESIAN_POINT('Ctrl Pts',(-21.8888646933687,26.3117602244235,6.64088070945616));
#44744=CARTESIAN_POINT('Ctrl Pts',(-21.8991179127129,26.317911095361,6.64161691353699));
#44745=CARTESIAN_POINT('Ctrl Pts',(-21.9058790208888,26.3219334675595,6.64210222149582));
#44746=CARTESIAN_POINT('Ctrl Pts',(-21.9212037649373,26.3309747766079,6.643201903838));
#44747=CARTESIAN_POINT('Ctrl Pts',(-21.9297759663029,26.3359789693221,6.64381680996049));
#44748=CARTESIAN_POINT('Ctrl Pts',(-21.9571149497055,26.3517697544605,6.64577727768757));
#44749=CARTESIAN_POINT('Ctrl Pts',(-21.9759670438212,26.3624067362789,6.64712822195695));
#44750=CARTESIAN_POINT('Ctrl Pts',(-22.0214287485067,26.387457348192,6.65038429417828));
#44751=CARTESIAN_POINT('Ctrl Pts',(-22.0481352518283,26.4016866825092,6.6522956913974));
#44752=CARTESIAN_POINT('Ctrl Pts',(-22.0750360194354,26.4155367766617,6.65421995916067));
#44753=CARTESIAN_POINT('Origin',(-23.5502525316942,23.5502525316942,-77.3107734492734));
#44754=CARTESIAN_POINT('',(-22.075035838959,26.4155366837419,8.15244980096843));
#44755=CARTESIAN_POINT('',(-22.0750360380806,26.4155367862613,7.90859913775027));
#44756=CARTESIAN_POINT('',(-22.0750360153461,26.4155367745563,-77.3107734492734));
#44757=CARTESIAN_POINT('Ctrl Pts',(-22.075035838959,26.4155366837419,8.15244980096843));
#44758=CARTESIAN_POINT('Ctrl Pts',(-22.0034785551328,26.3786947881442,8.14702447166941));
#44759=CARTESIAN_POINT('Ctrl Pts',(-21.9332984506555,26.3391707970346,8.14163349505117));
#44760=CARTESIAN_POINT('Ctrl Pts',(-21.8252269562421,26.2728511734628,8.13329272431396));
#44761=CARTESIAN_POINT('Ctrl Pts',(-21.786330880127,26.2478139239187,8.1302826068504));
#44762=CARTESIAN_POINT('Ctrl Pts',(-21.7199938119459,26.2030643697733,8.12515193354574));
#44763=CARTESIAN_POINT('Ctrl Pts',(-21.6922994345911,26.183742259056,8.12301095921678));
#44764=CARTESIAN_POINT('Ctrl Pts',(-21.6611656691945,26.1612848432148,8.12060991974254));
#44765=CARTESIAN_POINT('Ctrl Pts',(-21.6574246057767,26.1585740895882,8.12032150571276));
#44766=CARTESIAN_POINT('Ctrl Pts',(-21.6521603880067,26.1547423767257,8.11991581783683));
#44767=CARTESIAN_POINT('Ctrl Pts',(-21.6506323945351,26.1536281237562,8.11979808089806));
#44768=CARTESIAN_POINT('Ctrl Pts',(-21.6475639833635,26.151386418014,8.11956168767697));
#44769=CARTESIAN_POINT('Ctrl Pts',(-21.6460235827623,26.150258938731,8.11944303309373));
#44770=CARTESIAN_POINT('Ctrl Pts',(-21.6430645304162,26.1480890526141,8.11921514048876));
#44771=CARTESIAN_POINT('Ctrl Pts',(-21.641645733673,26.1470468539747,8.11910588816428));
#44772=CARTESIAN_POINT('Ctrl Pts',(-21.6382919891239,26.1445790767582,8.11884767615582));
#44773=CARTESIAN_POINT('Ctrl Pts',(-21.6363577773655,26.1431524927823,8.11869878705824));
#44774=CARTESIAN_POINT('Ctrl Pts',(-21.6306094644303,26.1389028699247,8.11825638475496));
#44775=CARTESIAN_POINT('Ctrl Pts',(-21.6267999789832,26.1360735536261,8.11796330815195));
#44776=CARTESIAN_POINT('Ctrl Pts',(-21.5921129226067,26.1101923056816,8.11529557495283));
#44777=CARTESIAN_POINT('Ctrl Pts',(-21.5616431988227,26.086595493376,8.11295841195184));
#44778=CARTESIAN_POINT('Ctrl Pts',(-21.4450829803222,25.992934989046,8.10401024671193));
#44779=CARTESIAN_POINT('Ctrl Pts',(-21.3622040773661,25.9189832312385,8.09763032769996));
#44780=CARTESIAN_POINT('Ctrl Pts',(-21.1889049707653,25.7474764031931,8.083834188344));
#44781=CARTESIAN_POINT('Ctrl Pts',(-21.1003730628055,25.6483104721367,8.07647111430951));
#44782=CARTESIAN_POINT('Ctrl Pts',(-20.9380246428854,25.4421256121732,8.06175781139711));
#44783=CARTESIAN_POINT('Ctrl Pts',(-20.8640600785651,25.335549326988,8.0544244944145));
#44784=CARTESIAN_POINT('Ctrl Pts',(-20.7654005838118,25.1733205167901,8.04336893801605));
#44785=CARTESIAN_POINT('Ctrl Pts',(-20.7355360632764,25.1209595684009,8.03981695791077));
#44786=CARTESIAN_POINT('Ctrl Pts',(-20.6875052776914,25.0309745404327,8.03371822997947));
#44787=CARTESIAN_POINT('Ctrl Pts',(-20.6685700278105,24.9937778017171,8.03119885074567));
#44788=CARTESIAN_POINT('Ctrl Pts',(-20.6469291462226,24.9491423911917,8.02817387231961));
#44789=CARTESIAN_POINT('Ctrl Pts',(-20.6435211652808,24.9420471578538,8.02769297280075));
#44790=CARTESIAN_POINT('Ctrl Pts',(-20.6383728988901,24.9312273565767,8.02695952871431));
#44791=CARTESIAN_POINT('Ctrl Pts',(-20.6366136734484,24.9275117906461,8.02670764276028));
#44792=CARTESIAN_POINT('Ctrl Pts',(-20.6335722724139,24.9210563027633,8.02626997638259));
#44793=CARTESIAN_POINT('Ctrl Pts',(-20.6322868334148,24.9183179165415,8.02608430942372));
#44794=CARTESIAN_POINT('Ctrl Pts',(-20.6296208548398,24.9126176989727,8.02569780080093));
#44795=CARTESIAN_POINT('Ctrl Pts',(-20.6282409612172,24.9096555707982,8.02549693702364));
#44796=CARTESIAN_POINT('Ctrl Pts',(-20.6248851213634,24.9024230895018,8.02500646143268));
#44797=CARTESIAN_POINT('Ctrl Pts',(-20.6229140218751,24.8981505068359,8.02471668237714));
#44798=CARTESIAN_POINT('Ctrl Pts',(-20.6154643694813,24.8819091212375,8.02361501485377));
#44799=CARTESIAN_POINT('Ctrl Pts',(-20.610049864884,24.869911237329,8.02280092103195));
#44800=CARTESIAN_POINT('Ctrl Pts',(-20.5175003285324,24.6614355439169,8.00864952970832));
#44801=CARTESIAN_POINT('Ctrl Pts',(-20.450179587129,24.4567999048437,7.99461540490779));
#44802=CARTESIAN_POINT('Ctrl Pts',(-20.3678952238628,24.0852160581386,7.96905764102781));
#44803=CARTESIAN_POINT('Ctrl Pts',(-20.3445991609664,23.9208864770235,7.95774659864501));
#44804=CARTESIAN_POINT('Ctrl Pts',(-20.3284826437955,23.6683369826585,7.94081604118686));
#44805=CARTESIAN_POINT('Ctrl Pts',(-20.326465406691,23.5809806549005,7.93504531829204));
#44806=CARTESIAN_POINT('Ctrl Pts',(-20.3286796376527,23.4549433767502,7.92693592404091));
#44807=CARTESIAN_POINT('Ctrl Pts',(-20.3300567223239,23.4162561472129,7.92447636253162));
#44808=CARTESIAN_POINT('Ctrl Pts',(-20.3323856576079,23.3728461708287,7.92175681284996));
#44809=CARTESIAN_POINT('Ctrl Pts',(-20.332651294238,23.3680918508868,7.9214595073092));
#44810=CARTESIAN_POINT('Ctrl Pts',(-20.3330658667313,23.3609558878315,7.92101410200949));
#44811=CARTESIAN_POINT('Ctrl Pts',(-20.3332069106098,23.3585738199304,7.92086555994366));
#44812=CARTESIAN_POINT('Ctrl Pts',(-20.3334528044039,23.354497690627,7.92061162000901));
#44813=CARTESIAN_POINT('Ctrl Pts',(-20.3335563468899,23.3528035559662,7.92050614799976));
#44814=CARTESIAN_POINT('Ctrl Pts',(-20.3337723884344,23.349314017206,7.92028904693828));
#44815=CARTESIAN_POINT('Ctrl Pts',(-20.3338850521282,23.3475186297013,7.92017742756349));
#44816=CARTESIAN_POINT('Ctrl Pts',(-20.3341937695832,23.3426639999473,7.91987582990135));
#44817=CARTESIAN_POINT('Ctrl Pts',(-20.3343926857691,23.3396049316202,7.91968601382583));
#44818=CARTESIAN_POINT('Ctrl Pts',(-20.3351451055483,23.3282832133299,7.91898433742694));
#44819=CARTESIAN_POINT('Ctrl Pts',(-20.3357260972516,23.3200223299647,7.91847401501613));
#44820=CARTESIAN_POINT('Ctrl Pts',(-20.3460981958381,23.1802462894014,7.90986588144374));
#44821=CARTESIAN_POINT('Ctrl Pts',(-20.363922501921,23.0494331319363,7.90220726893785));
#44822=CARTESIAN_POINT('Ctrl Pts',(-20.4330029498787,22.7029789915037,7.88213167768738));
#44823=CARTESIAN_POINT('Ctrl Pts',(-20.4985384198102,22.490930559686,7.87002825248174));
#44824=CARTESIAN_POINT('Ctrl Pts',(-20.627503922865,22.1881733139795,7.85124677101036));
#44825=CARTESIAN_POINT('Ctrl Pts',(-20.6746532251314,22.0912650184146,7.84499425214507));
#44826=CARTESIAN_POINT('Ctrl Pts',(-20.7498366178128,21.954595920712,7.83569787113862));
#44827=CARTESIAN_POINT('Ctrl Pts',(-20.7740581885332,21.9128173735767,7.8327883686596));
#44828=CARTESIAN_POINT('Ctrl Pts',(-20.8033428022954,21.8648245422401,7.82936057211804));
#44829=CARTESIAN_POINT('Ctrl Pts',(-20.807502331411,21.8580640356423,7.82887570745612));
#44830=CARTESIAN_POINT('Ctrl Pts',(-20.8139154804342,21.847726473771,7.82813118407977));
#44831=CARTESIAN_POINT('Ctrl Pts',(-20.8161512545446,21.8441383379702,7.82787218504296));
#44832=CARTESIAN_POINT('Ctrl Pts',(-20.8200070481755,21.8379773182944,7.82742647202648));
#44833=CARTESIAN_POINT('Ctrl Pts',(-20.8216236641268,21.8354023021785,7.82723988438298));
#44834=CARTESIAN_POINT('Ctrl Pts',(-20.8249590426426,21.8301062241432,7.82685550533873));
#44835=CARTESIAN_POINT('Ctrl Pts',(-20.8266782418755,21.8273854420555,7.82665769784231));
#44836=CARTESIAN_POINT('Ctrl Pts',(-20.8308245256808,21.8208453035152,7.82618139630988));
#44837=CARTESIAN_POINT('Ctrl Pts',(-20.8332555800786,21.8170284823127,7.82590275463257));
#44838=CARTESIAN_POINT('Ctrl Pts',(-20.8407333860387,21.8053425182306,7.82504756469418));
#44839=CARTESIAN_POINT('Ctrl Pts',(-20.8458063113168,21.7974902563447,7.82447003969262));
#44840=CARTESIAN_POINT('Ctrl Pts',(-20.9048779277582,21.7069216825903,7.81777505465706));
#44841=CARTESIAN_POINT('Ctrl Pts',(-20.9626126369707,21.6267162736115,7.81151671244625));
#44842=CARTESIAN_POINT('Ctrl Pts',(-21.0663779758242,21.4957068621098,7.80070286483037));
#44843=CARTESIAN_POINT('Ctrl Pts',(-21.1105138772957,21.4434860427505,7.79621962943361));
#44844=CARTESIAN_POINT('Ctrl Pts',(-21.2936074916002,21.2403279544188,7.77809009232828));
#44845=CARTESIAN_POINT('Ctrl Pts',(-21.4451725836988,21.1014105496273,7.76406242178501));
#44846=CARTESIAN_POINT('Ctrl Pts',(-21.671255655043,20.930788390186,7.74505161747657));
#44847=CARTESIAN_POINT('Ctrl Pts',(-21.7353129352484,20.886004522952,7.73985663355557));
#44848=CARTESIAN_POINT('Ctrl Pts',(-21.8462375964566,20.8143139704335,7.73125154447303));
#44849=CARTESIAN_POINT('Ctrl Pts',(-21.8922679606301,20.7861767893041,7.72778841364106));
#44850=CARTESIAN_POINT('Ctrl Pts',(-21.9444788401436,20.7560355324648,7.7239972638394));
#44851=CARTESIAN_POINT('Ctrl Pts',(-21.9499809589547,20.752880786227,7.72359941314159));
#44852=CARTESIAN_POINT('Ctrl Pts',(-21.959726182036,20.7473313356938,7.7228977474691));
#44853=CARTESIAN_POINT('Ctrl Pts',(-21.9639654497386,20.7449299844085,7.72259351488441));
#44854=CARTESIAN_POINT('Ctrl Pts',(-21.9702842871635,20.7413695550443,7.72214154515304));
#44855=CARTESIAN_POINT('Ctrl Pts',(-21.9723596968909,20.740203166967,7.72199333748785));
#44856=CARTESIAN_POINT('Ctrl Pts',(-21.9759228773562,20.7382058382954,7.72173930184025));
#44857=CARTESIAN_POINT('Ctrl Pts',(-21.9774100151513,20.7373737777139,7.72163340097217));
#44858=CARTESIAN_POINT('Ctrl Pts',(-21.9804551039666,20.7356732061318,7.72141681119816));
#44859=CARTESIAN_POINT('Ctrl Pts',(-21.9820131129378,20.7348048107303,7.72130612987596));
#44860=CARTESIAN_POINT('Ctrl Pts',(-21.9857492929873,20.7327264205352,7.7210410348226));
#44861=CARTESIAN_POINT('Ctrl Pts',(-21.9879281519934,20.731517655251,7.72088670084779));
#44862=CARTESIAN_POINT('Ctrl Pts',(-21.9957946668233,20.7271654733145,7.72033043894199));
#44863=CARTESIAN_POINT('Ctrl Pts',(-22.0014904752483,20.7240367071152,7.71992944961804));
#44864=CARTESIAN_POINT('Ctrl Pts',(-22.0911033929641,20.6751636709981,7.71364786378641));
#44865=CARTESIAN_POINT('Ctrl Pts',(-22.1770148744117,20.6331521548447,7.70799980258374));
#44866=CARTESIAN_POINT('Ctrl Pts',(-22.5166598226966,20.4854009270515,7.68660547369846));
#44867=CARTESIAN_POINT('Ctrl Pts',(-22.7816364414664,20.4084569896587,7.67177399100078));
#44868=CARTESIAN_POINT('Ctrl Pts',(-23.1765186499219,20.3468131474472,7.64885285222863));
#44869=CARTESIAN_POINT('Ctrl Pts',(-23.3008592335329,20.334743496168,7.64153882714288));
#44870=CARTESIAN_POINT('Ctrl Pts',(-23.4459210268486,20.3291274172142,7.6327577877768));
#44871=CARTESIAN_POINT('Ctrl Pts',(-23.4662717785913,20.3285326075616,7.63152039310426));
#44872=CARTESIAN_POINT('Ctrl Pts',(-23.492661497411,20.3280114992223,7.62990826175459));
#44873=CARTESIAN_POINT('Ctrl Pts',(-23.4986968412881,20.3279092835938,7.62953905511939));
#44874=CARTESIAN_POINT('Ctrl Pts',(-23.508440969668,20.3277716377274,7.62894212952983));
#44875=CARTESIAN_POINT('Ctrl Pts',(-23.5121496101861,20.3277256526922,7.62871474227271));
#44876=CARTESIAN_POINT('Ctrl Pts',(-23.5192252448072,20.3276501349483,7.62828053829919));
#44877=CARTESIAN_POINT('Ctrl Pts',(-23.522592224077,20.327619476677,7.62807375721324));
#44878=CARTESIAN_POINT('Ctrl Pts',(-23.5302847954498,20.327561487932,7.62760094780115));
#44879=CARTESIAN_POINT('Ctrl Pts',(-23.5346104001501,20.3275375896825,7.62733481205746));
#44880=CARTESIAN_POINT('Ctrl Pts',(-23.547857126271,20.3274910742487,7.62651896217254));
#44881=CARTESIAN_POINT('Ctrl Pts',(-23.5567782481965,20.3274967913346,7.62596835957772));
#44882=CARTESIAN_POINT('Ctrl Pts',(-23.5929260002519,20.3276700493614,7.62373257010375));
#44883=CARTESIAN_POINT('Ctrl Pts',(-23.6201493923751,20.3281455757059,7.62203774741171));
#44884=CARTESIAN_POINT('Ctrl Pts',(-23.6552082448343,20.329202475085,7.61984034476223));
#44885=CARTESIAN_POINT('Ctrl Pts',(-23.663052708489,20.3294676448599,7.61934772067625));
#44886=CARTESIAN_POINT('Ctrl Pts',(-23.6803118992806,20.3301141952762,7.61826174788554));
#44887=CARTESIAN_POINT('Ctrl Pts',(-23.6897260552538,20.3305082129695,7.61766801122811));
#44888=CARTESIAN_POINT('Ctrl Pts',(-23.7007641282942,20.331018698798,7.61697021886843));
#44889=CARTESIAN_POINT('Ctrl Pts',(-23.7023899287517,20.3310951226855,7.61686739919075));
#44890=CARTESIAN_POINT('Ctrl Pts',(-23.7120382858864,20.3315559878299,7.61625696538053));
#44891=CARTESIAN_POINT('Ctrl Pts',(-23.7200593842456,20.3319691845192,7.6157484690072));
#44892=CARTESIAN_POINT('Ctrl Pts',(-23.7399088283264,20.3330661167194,7.61448758696714));
#44893=CARTESIAN_POINT('Ctrl Pts',(-23.7517350376127,20.3337851008907,7.61373413456991));
#44894=CARTESIAN_POINT('Ctrl Pts',(-24.0386171782483,20.3528147147812,7.59540246237311));
#44895=CARTESIAN_POINT('Ctrl Pts',(-24.3101590117772,20.4062748374603,7.57669130377256));
#44896=CARTESIAN_POINT('Ctrl Pts',(-24.7304849340708,20.5467114161775,7.54676948622247));
#44897=CARTESIAN_POINT('Ctrl Pts',(-24.885086287283,20.6121507292481,7.53557449906745));
#44898=CARTESIAN_POINT('Ctrl Pts',(-25.0406574866387,20.6928291511576,7.52457510903283));
#44899=CARTESIAN_POINT('Ctrl Pts',(-25.0473908972771,20.6963513381614,7.52409960162688));
#44900=CARTESIAN_POINT('Ctrl Pts',(-25.05663775305,20.7012300180099,7.5234474439656));
#44901=CARTESIAN_POINT('Ctrl Pts',(-25.05916187744,20.7025660487625,7.52326951088678));
#44902=CARTESIAN_POINT('Ctrl Pts',(-25.0634205836321,20.7048274537639,7.52296945345086));
#44903=CARTESIAN_POINT('Ctrl Pts',(-25.0651560945862,20.7057510599584,7.5228472163844));
#44904=CARTESIAN_POINT('Ctrl Pts',(-25.0685749050392,20.7075745027444,7.52260650520676));
#44905=CARTESIAN_POINT('Ctrl Pts',(-25.070258250415,20.7084742467528,7.52248802544948));
#44906=CARTESIAN_POINT('Ctrl Pts',(-25.0739708545963,20.7104628672172,7.52222680768948));
#44907=CARTESIAN_POINT('Ctrl Pts',(-25.0759997510971,20.7115524262621,7.52208411343012));
#44908=CARTESIAN_POINT('Ctrl Pts',(-25.0830980543048,20.7153741692392,7.52158508097397));
#44909=CARTESIAN_POINT('Ctrl Pts',(-25.0881613431049,20.7181177864706,7.52122947031888));
#44910=CARTESIAN_POINT('Ctrl Pts',(-25.1399375765307,20.7463532914741,7.51759641235279));
#44911=CARTESIAN_POINT('Ctrl Pts',(-25.1860229984064,20.7729867391002,7.51439062244875));
#44912=CARTESIAN_POINT('Ctrl Pts',(-25.3145325510243,20.8515637063047,7.50547020951547));
#44913=CARTESIAN_POINT('Ctrl Pts',(-25.3952946799141,20.9061217097825,7.49988618709235));
#44914=CARTESIAN_POINT('Ctrl Pts',(-25.5264491598719,21.0036618303362,7.49064266265321));
#44915=CARTESIAN_POINT('Ctrl Pts',(-25.5782091334936,21.0446847986799,7.48694526653462));
#44916=CARTESIAN_POINT('Ctrl Pts',(-25.7309918230604,21.1736124847479,7.47576928506367));
#44917=CARTESIAN_POINT('Ctrl Pts',(-25.8278286266458,21.2662456859885,7.46831524581369));
#44918=CARTESIAN_POINT('Ctrl Pts',(-25.9851839517236,21.4367578644358,7.45509907446572));
#44919=CARTESIAN_POINT('Ctrl Pts',(-26.0484124439881,21.5118842151716,7.4494249050375));
#44920=CARTESIAN_POINT('Ctrl Pts',(-26.1468356744202,21.6402981327042,7.43985126312269));
#44921=CARTESIAN_POINT('Ctrl Pts',(-26.1840523075463,21.6919555415958,7.43603141774321));
#44922=CARTESIAN_POINT('Ctrl Pts',(-26.2244194192409,21.7516365127145,7.43163947199003));
#44923=CARTESIAN_POINT('Ctrl Pts',(-26.2290984578448,21.7586128837675,7.43112640516336));
#44924=CARTESIAN_POINT('Ctrl Pts',(-26.236087455396,21.7691219524947,7.43035399016273));
#44925=CARTESIAN_POINT('Ctrl Pts',(-26.2384178621609,21.772641063081,7.43009541297855));
#44926=CARTESIAN_POINT('Ctrl Pts',(-26.2424145132216,21.7787021751243,7.42965018249831));
#44927=CARTESIAN_POINT('Ctrl Pts',(-26.2440840911412,21.7812419806043,7.42946365477132));
#44928=CARTESIAN_POINT('Ctrl Pts',(-26.2475156193518,21.7864782338362,7.42907917262162));
#44929=CARTESIAN_POINT('Ctrl Pts',(-26.2492771246312,21.7891749682608,7.42888120176989));
#44930=CARTESIAN_POINT('Ctrl Pts',(-26.254008415624,21.7964419974879,7.42834783010748));
#44931=CARTESIAN_POINT('Ctrl Pts',(-26.2569706451959,21.8010171778222,7.42801214717339));
#44932=CARTESIAN_POINT('Ctrl Pts',(-26.2677902865465,21.8178214641674,7.42677962210954));
#44933=CARTESIAN_POINT('Ctrl Pts',(-26.2755764511271,21.8300960342168,7.42588013101528));
#44934=CARTESIAN_POINT('Ctrl Pts',(-26.2938036416582,21.8592648641696,7.42374430242491));
#44935=CARTESIAN_POINT('Ctrl Pts',(-26.3041719692178,21.8762036411817,7.42250531922469));
#44936=CARTESIAN_POINT('Ctrl Pts',(-26.5008151727119,22.2042315893919,7.39853399703484));
#44937=CARTESIAN_POINT('Ctrl Pts',(-26.6333925004005,22.5444195078288,7.37361781901645));
#44938=CARTESIAN_POINT('Ctrl Pts',(-26.7309806132763,23.0176419960814,7.34131964240364));
#44939=CARTESIAN_POINT('Ctrl Pts',(-26.7487086678329,23.1372258858783,7.33338983569784));
#44940=CARTESIAN_POINT('Ctrl Pts',(-26.7602543032145,23.2638158975588,7.32542316972101));
#44941=CARTESIAN_POINT('Ctrl Pts',(-26.7608085721551,23.270096805,7.3250290027055));
#44942=CARTESIAN_POINT('Ctrl Pts',(-26.7615700264782,23.2790246594217,7.32447033625397));
#44943=CARTESIAN_POINT('Ctrl Pts',(-26.7617923753193,23.2816702464746,7.32430498810685));
#44944=CARTESIAN_POINT('Ctrl Pts',(-26.7621693599687,23.2862231536489,7.32402078297492));
#44945=CARTESIAN_POINT('Ctrl Pts',(-26.7623255664406,23.2881303392919,7.32390183674331));
#44946=CARTESIAN_POINT('Ctrl Pts',(-26.7626217575744,23.2917866766836,7.32367400424059));
#44947=CARTESIAN_POINT('Ctrl Pts',(-26.7627620121057,23.293535800857,7.32356510264455));
#44948=CARTESIAN_POINT('Ctrl Pts',(-26.7630892205207,23.2976587012696,7.32330861674754));
#44949=CARTESIAN_POINT('Ctrl Pts',(-26.7632749726379,23.3000325758239,7.32316110076436));
#44950=CARTESIAN_POINT('Ctrl Pts',(-26.7638163312105,23.3070510360716,7.3227254393449));
#44951=CARTESIAN_POINT('Ctrl Pts',(-26.7641645008306,23.31169621482,7.32243771205807));
#44952=CARTESIAN_POINT('Ctrl Pts',(-26.7671254205255,23.3523833230073,7.31992277500548));
#44953=CARTESIAN_POINT('Ctrl Pts',(-26.7691420000244,23.3884679040528,7.31772850286132));
#44954=CARTESIAN_POINT('Ctrl Pts',(-26.7707584802383,23.4298896357098,7.3152433469209));
#44955=CARTESIAN_POINT('Ctrl Pts',(-26.7709525373825,23.4351992160073,7.31492542495245));
#44956=CARTESIAN_POINT('Ctrl Pts',(-26.7711818205749,23.4419285036839,7.31452327111515));
#44957=CARTESIAN_POINT('Ctrl Pts',(-26.7712292387856,23.4433477544264,7.31443849798091));
#44958=CARTESIAN_POINT('Ctrl Pts',(-26.771406450904,23.448758966201,7.31411544658448));
#44959=CARTESIAN_POINT('Ctrl Pts',(-26.7715297623108,23.4527511527492,7.31387745428242));
#44960=CARTESIAN_POINT('Ctrl Pts',(-26.7716929991642,23.4583746791862,7.31354268035651));
#44961=CARTESIAN_POINT('Ctrl Pts',(-26.7717391072137,23.4600058198219,7.31344563267206));
#44962=CARTESIAN_POINT('Ctrl Pts',(-26.771984204172,23.468916081101,7.31291580121302));
#44963=CARTESIAN_POINT('Ctrl Pts',(-26.7721597622356,23.476195883072,7.31248401830316));
#44964=CARTESIAN_POINT('Ctrl Pts',(-26.7723898797889,23.4872994130233,7.31182702886601));
#44965=CARTESIAN_POINT('Ctrl Pts',(-26.7724623089478,23.4911227020264,7.31160109420439));
#44966=CARTESIAN_POINT('Ctrl Pts',(-26.7728346105248,23.5128138284192,7.31032085568844));
#44967=CARTESIAN_POINT('Ctrl Pts',(-26.7729926719099,23.5306841023086,7.30927222495788));
#44968=CARTESIAN_POINT('Ctrl Pts',(-26.7730393907041,23.6193840350769,7.30409354850758));
#44969=CARTESIAN_POINT('Ctrl Pts',(-26.7707416864332,23.6901987382377,7.30004191843296));
#44970=CARTESIAN_POINT('Ctrl Pts',(-26.7433386453863,24.1085812604084,7.27630775675397));
#44971=CARTESIAN_POINT('Ctrl Pts',(-26.6643392046655,24.4502482074331,7.2574565837971));
#44972=CARTESIAN_POINT('Ctrl Pts',(-26.5242839521232,24.7918996148428,7.23513201115579));
#44973=CARTESIAN_POINT('Ctrl Pts',(-26.5162068814347,24.8110717623944,7.23386804110642));
#44974=CARTESIAN_POINT('Ctrl Pts',(-26.5054415844893,24.8359488236887,7.23221285620487));
#44975=CARTESIAN_POINT('Ctrl Pts',(-26.5029213184341,24.8417262356189,7.23182739024658));
#44976=CARTESIAN_POINT('Ctrl Pts',(-26.4990188164999,24.8506011252803,7.23123360381595));
#44977=CARTESIAN_POINT('Ctrl Pts',(-26.497648602715,24.8537038992718,7.2310256959427));
#44978=CARTESIAN_POINT('Ctrl Pts',(-26.4949314578639,24.8598305332848,7.23061454735716));
#44979=CARTESIAN_POINT('Ctrl Pts',(-26.4935847608902,24.8628544930381,7.23041131488654));
#44980=CARTESIAN_POINT('Ctrl Pts',(-26.4905907655944,24.8695496263277,7.2299606861103));
#44981=CARTESIAN_POINT('Ctrl Pts',(-26.4889412479145,24.8732197960546,7.22971321364366));
#44982=CARTESIAN_POINT('Ctrl Pts',(-26.4842132736953,24.8836870460961,7.22900615121549));
#44983=CARTESIAN_POINT('Ctrl Pts',(-26.4811180936343,24.8904765040716,7.2285459849923));
#44984=CARTESIAN_POINT('Ctrl Pts',(-26.4613270243664,24.9334929331668,7.22562062467509));
#44985=CARTESIAN_POINT('Ctrl Pts',(-26.4439839503859,24.9694167068045,7.2231330916337));
#44986=CARTESIAN_POINT('Ctrl Pts',(-26.3904858614386,25.0751704749775,7.21567282935285));
#44987=CARTESIAN_POINT('Ctrl Pts',(-26.352439387745,25.144005092115,7.21063488280423));
#44988=CARTESIAN_POINT('Ctrl Pts',(-26.234180849252,25.3406132947755,7.19570086808431));
#44989=CARTESIAN_POINT('Ctrl Pts',(-26.1474766539702,25.4642225875008,7.18560062836074));
#44990=CARTESIAN_POINT('Ctrl Pts',(-25.9845755879772,25.6649125468504,7.16812864592451));
#44991=CARTESIAN_POINT('Ctrl Pts',(-25.9125548914997,25.7450745757454,7.1608162400925));
#44992=CARTESIAN_POINT('Ctrl Pts',(-25.7716525556992,25.8869182971149,7.14739772083273));
#44993=CARTESIAN_POINT('Ctrl Pts',(-25.7038649688071,25.9495401602419,7.14127580285021));
#44994=CARTESIAN_POINT('Ctrl Pts',(-25.5991177561338,26.0382832873199,7.13240364419521));
#44995=CARTESIAN_POINT('Ctrl Pts',(-25.5641476221196,26.0666731700698,7.12953250510165));
#44996=CARTESIAN_POINT('Ctrl Pts',(-25.5243008174668,26.09765914896,7.1263719707721));
#44997=CARTESIAN_POINT('Ctrl Pts',(-25.5200014298373,26.1009850514901,7.12603237490713));
#44998=CARTESIAN_POINT('Ctrl Pts',(-25.5138826580851,26.1056936894792,7.12555110823747));
#44999=CARTESIAN_POINT('Ctrl Pts',(-25.512070216707,26.1070853684322,7.1254088051807));
#45000=CARTESIAN_POINT('Ctrl Pts',(-25.5087448323276,26.1096331396472,7.12514817979121));
#45001=CARTESIAN_POINT('Ctrl Pts',(-25.5072323426977,26.1107898205051,7.12502981540053));
#45002=CARTESIAN_POINT('Ctrl Pts',(-25.5041511525431,26.1131418448668,7.12478904774322));
#45003=CARTESIAN_POINT('Ctrl Pts',(-25.5025823797302,26.1143370889286,7.12466665159665));
#45004=CARTESIAN_POINT('Ctrl Pts',(-25.4986686760882,26.117313255773,7.12436177261338));
#45005=CARTESIAN_POINT('Ctrl Pts',(-25.496322393707,26.1190924109343,7.1241794157452));
#45006=CARTESIAN_POINT('Ctrl Pts',(-25.4874652575031,26.1257895621207,7.12349259090087));
#45007=CARTESIAN_POINT('Ctrl Pts',(-25.4809381003474,26.1306860957576,7.12298962947317));
#45008=CARTESIAN_POINT('Ctrl Pts',(-25.3616965696974,26.2194328188426,7.11385770962764));
#45009=CARTESIAN_POINT('Ctrl Pts',(-25.243620223074,26.2958617517828,7.10572850397359));
#45010=CARTESIAN_POINT('Ctrl Pts',(-24.8131401625233,26.5361306182987,7.07778981894577));
#45011=CARTESIAN_POINT('Ctrl Pts',(-24.4793033421325,26.6562497109241,7.05875248575931));
#45012=CARTESIAN_POINT('Ctrl Pts',(-24.1124581992876,26.7236518410585,7.03619787995373));
#45013=CARTESIAN_POINT('Ctrl Pts',(-24.0922473063135,26.727166131933,7.03495139778635));
#45014=CARTESIAN_POINT('Ctrl Pts',(-24.0658186033756,26.7315020479564,7.03331597216524));
#45015=CARTESIAN_POINT('Ctrl Pts',(-24.0596296974438,26.732498870544,7.03293260849408));
#45016=CARTESIAN_POINT('Ctrl Pts',(-24.0500945604591,26.734006128692,7.03234135354054));
#45017=CARTESIAN_POINT('Ctrl Pts',(-24.0467503436351,26.7345293636791,7.03213386920611));
#45018=CARTESIAN_POINT('Ctrl Pts',(-24.0401680270289,26.735548609184,7.0317252534834));
#45019=CARTESIAN_POINT('Ctrl Pts',(-24.0369299824095,26.7360449531618,7.03152413295271));
#45020=CARTESIAN_POINT('Ctrl Pts',(-24.0297970907488,26.7371271905914,7.0310808524472));
#45021=CARTESIAN_POINT('Ctrl Pts',(-24.0259019193954,26.737710882073,7.03083862289382));
#45022=CARTESIAN_POINT('Ctrl Pts',(-24.0149045596416,26.7393382291663,7.03015427090614));
#45023=CARTESIAN_POINT('Ctrl Pts',(-24.0077999731732,26.74036529308,7.02971162282511));
#45024=CARTESIAN_POINT('Ctrl Pts',(-23.9919081484274,26.7426084913474,7.02872026265327));
#45025=CARTESIAN_POINT('Ctrl Pts',(-23.9831192262033,26.7438120941853,7.02817115624149));
#45026=CARTESIAN_POINT('Ctrl Pts',(-23.8085636046649,26.7669828774427,7.01724844224511));
#45027=CARTESIAN_POINT('Ctrl Pts',(-23.6413686860704,26.7760486290695,7.00646168092928));
#45028=CARTESIAN_POINT('Ctrl Pts',(-23.2601015975465,26.767054353661,6.98115145776986));
#45029=CARTESIAN_POINT('Ctrl Pts',(-23.0469962430431,26.740663942086,6.96647516883323));
#45030=CARTESIAN_POINT('Ctrl Pts',(-22.7871915497385,26.6817986482123,6.94865493893199));
#45031=CARTESIAN_POINT('Ctrl Pts',(-22.7365606340584,26.6690261854752,6.9451883674089));
#45032=CARTESIAN_POINT('Ctrl Pts',(-22.6617747163008,26.648214879732,6.94009718016781));
#45033=CARTESIAN_POINT('Ctrl Pts',(-22.6373698040873,26.6411114314313,6.9384404819557));
#45034=CARTESIAN_POINT('Ctrl Pts',(-22.6030687041969,26.6306858140148,6.93612100312859));
#45035=CARTESIAN_POINT('Ctrl Pts',(-22.5931012663745,26.6276033194611,6.93544807471076));
#45036=CARTESIAN_POINT('Ctrl Pts',(-22.5478950703297,26.6133821250359,6.93240153711876));
#45037=CARTESIAN_POINT('Ctrl Pts',(-22.5128327538376,26.6016856183889,6.93005368677008));
#45038=CARTESIAN_POINT('Ctrl Pts',(-22.4731291530991,26.5876773000436,6.92741847135614));
#45039=CARTESIAN_POINT('Ctrl Pts',(-22.4682847785286,26.5859550497417,6.92709734017924));
#45040=CARTESIAN_POINT('Ctrl Pts',(-22.4611358794341,26.583394218778,6.92662405741832));
#45041=CARTESIAN_POINT('Ctrl Pts',(-22.4588281879092,26.5825645997448,6.9264713746471));
#45042=CARTESIAN_POINT('Ctrl Pts',(-22.454746845817,26.5810920876276,6.92620151308045));
#45043=CARTESIAN_POINT('Ctrl Pts',(-22.4529728116768,26.5804502707391,6.92608426965036));
#45044=CARTESIAN_POINT('Ctrl Pts',(-22.4492718578246,26.5791076491197,6.92583979908717));
#45045=CARTESIAN_POINT('Ctrl Pts',(-22.4473450471248,26.5784065646202,6.92571258932958));
#45046=CARTESIAN_POINT('Ctrl Pts',(-22.4423195062066,26.5765725509815,6.92538097245901));
#45047=CARTESIAN_POINT('Ctrl Pts',(-22.4392218343448,26.5754366976392,6.92517674109285));
#45048=CARTESIAN_POINT('Ctrl Pts',(-22.4258128376956,26.5704965173563,6.9242934032633));
#45049=CARTESIAN_POINT('Ctrl Pts',(-22.4155191077822,26.5666441546895,6.92361714779844));
#45050=CARTESIAN_POINT('Ctrl Pts',(-22.3413421523693,26.5384504478529,6.91875609895471));
#45051=CARTESIAN_POINT('Ctrl Pts',(-22.2782227337624,26.5121324854871,6.91468441294332));
#45052=CARTESIAN_POINT('Ctrl Pts',(-22.1684519854658,26.4622057246811,6.90763841321722));
#45053=CARTESIAN_POINT('Ctrl Pts',(-22.1214557159561,26.4394363613025,6.90463354385769));
#45054=CARTESIAN_POINT('Ctrl Pts',(-22.0750360103879,26.4155367720035,6.90165778540197));
#45055=CARTESIAN_POINT('',(-26.7730018526427,23.548160445141,7.06183203780204));
#45056=CARTESIAN_POINT('Ctrl Pts',(-22.0750360194354,26.4155367766617,6.65421995916067));
#45057=CARTESIAN_POINT('Ctrl Pts',(-22.1030069891242,26.4299378736632,6.656220780701));
#45058=CARTESIAN_POINT('Ctrl Pts',(-22.1311879873181,26.443928955527,6.65823551916694));
#45059=CARTESIAN_POINT('Ctrl Pts',(-22.2698207253827,26.5102438312251,6.66814175552328));
#45060=CARTESIAN_POINT('Ctrl Pts',(-22.3829711956814,26.5566628635125,6.67621724682854));
#45061=CARTESIAN_POINT('Ctrl Pts',(-22.7680281775915,26.6896097419607,6.70353224301071));
#45062=CARTESIAN_POINT('Ctrl Pts',(-23.0487452019916,26.7464912030137,6.72328756031603));
#45063=CARTESIAN_POINT('Ctrl Pts',(-23.3489469742249,26.7667475076122,6.74232093593207));
#45064=CARTESIAN_POINT('Ctrl Pts',(-23.3646130508503,26.7676896895248,6.74330789747096));
#45065=CARTESIAN_POINT('Ctrl Pts',(-23.3838252289674,26.7687043455624,6.74451003094967));
#45066=CARTESIAN_POINT('Ctrl Pts',(-23.3873650250473,26.768885438032,6.7447311786681));
#45067=CARTESIAN_POINT('Ctrl Pts',(-23.3932145388186,26.7691750187581,6.74509605155091));
#45068=CARTESIAN_POINT('Ctrl Pts',(-23.3955240747743,26.7692868610578,6.7452399648297));
#45069=CARTESIAN_POINT('Ctrl Pts',(-23.3995114141946,26.7694756520919,6.74548816904159));
#45070=CARTESIAN_POINT('Ctrl Pts',(-23.4011891545659,26.7695537746745,6.74559252639276));
#45071=CARTESIAN_POINT('Ctrl Pts',(-23.4049566760875,26.7697262546619,6.74582669318417));
#45072=CARTESIAN_POINT('Ctrl Pts',(-23.4070464848073,26.7698198887673,6.74595646108593));
#45073=CARTESIAN_POINT('Ctrl Pts',(-23.4126173142883,26.7700640556095,6.74630206277365));
#45074=CARTESIAN_POINT('Ctrl Pts',(-23.4160985028903,26.7702109785436,6.74651769249859));
#45075=CARTESIAN_POINT('Ctrl Pts',(-23.4323524040536,26.7708705666097,6.74752294484868));
#45076=CARTESIAN_POINT('Ctrl Pts',(-23.4451280883677,26.7713128899038,6.74830864923604));
#45077=CARTESIAN_POINT('Ctrl Pts',(-23.752673581825,26.78012906517,6.76712330162036));
#45078=CARTESIAN_POINT('Ctrl Pts',(-24.0472633585529,26.7480838122956,6.78303742053867));
#45079=CARTESIAN_POINT('Ctrl Pts',(-24.4626704680579,26.6440146834101,6.80713810845837));
#45080=CARTESIAN_POINT('Ctrl Pts',(-24.5897737118816,26.6036541758098,6.81473648374602));
#45081=CARTESIAN_POINT('Ctrl Pts',(-24.7250805930496,26.5512586285551,6.82327708405909));
#45082=CARTESIAN_POINT('Ctrl Pts',(-24.7361300064408,26.5469095319005,6.82397783777911));
#45083=CARTESIAN_POINT('Ctrl Pts',(-24.7589111398375,26.5377970502987,6.82542967620588));
#45084=CARTESIAN_POINT('Ctrl Pts',(-24.7706393121888,26.5330253995509,6.82618100403714));
#45085=CARTESIAN_POINT('Ctrl Pts',(-24.7887419836199,26.5255356202542,6.82734690161485));
#45086=CARTESIAN_POINT('Ctrl Pts',(-24.7951364256011,26.5228658044241,6.82775993839653));
#45087=CARTESIAN_POINT('Ctrl Pts',(-24.8081991576987,26.5173622944666,6.82860620266664));
#45088=CARTESIAN_POINT('Ctrl Pts',(-24.8148665978886,26.5145266958936,6.82903948936594));
#45089=CARTESIAN_POINT('Ctrl Pts',(-24.8271305570639,26.5092620436475,6.82983897282051));
#45090=CARTESIAN_POINT('Ctrl Pts',(-24.8327298605759,26.5068395308615,6.83020495494202));
#45091=CARTESIAN_POINT('Ctrl Pts',(-24.8504286364795,26.4991224997318,6.83136487634342));
#45092=CARTESIAN_POINT('Ctrl Pts',(-24.8625023477292,26.4937695444361,6.83216073471482));
#45093=CARTESIAN_POINT('Ctrl Pts',(-24.8937707336715,26.4796758935613,6.83423404475359));
#45094=CARTESIAN_POINT('Ctrl Pts',(-24.9129128801452,26.4708208212571,6.83551532184514));
#45095=CARTESIAN_POINT('Ctrl Pts',(-24.9376916100922,26.4590616568412,6.83719005411216));
#45096=CARTESIAN_POINT('Ctrl Pts',(-24.9434087761467,26.4563277888824,6.83757759056231));
#45097=CARTESIAN_POINT('Ctrl Pts',(-24.9525199675906,26.4519378803179,6.83819700586523));
#45098=CARTESIAN_POINT('Ctrl Pts',(-24.9559192303687,26.4502926962846,6.83842850599436));
#45099=CARTESIAN_POINT('Ctrl Pts',(-24.9622779110586,26.4472013990284,6.83886231294264));
#45100=CARTESIAN_POINT('Ctrl Pts',(-24.9652380215858,26.4457567149387,6.83906456962158));
#45101=CARTESIAN_POINT('Ctrl Pts',(-24.9710960067254,26.4428865928116,6.83946544654088));
#45102=CARTESIAN_POINT('Ctrl Pts',(-24.9739939641428,26.4414613317436,6.83966406040624));
#45103=CARTESIAN_POINT('Ctrl Pts',(-24.9829153997715,26.4370569633072,6.84027642391676));
#45104=CARTESIAN_POINT('Ctrl Pts',(-24.9889316777197,26.4340633843064,6.84069068060906));
#45105=CARTESIAN_POINT('Ctrl Pts',(-25.0204752879332,26.4182446411655,6.84286954008035));
#45106=CARTESIAN_POINT('Ctrl Pts',(-25.0458399609375,26.405099611612,6.84464537157516));
#45107=CARTESIAN_POINT('Ctrl Pts',(-25.1159263914291,26.3675875340592,6.84962038337753));
#45108=CARTESIAN_POINT('Ctrl Pts',(-25.1602487393301,26.342495874761,6.85284503590439));
#45109=CARTESIAN_POINT('Ctrl Pts',(-25.2741246433576,26.2744158762107,6.8613407358109));
#45110=CARTESIAN_POINT('Ctrl Pts',(-25.3426665149479,26.2298143109516,6.86666639476673));
#45111=CARTESIAN_POINT('Ctrl Pts',(-25.6895010385416,25.9848564471684,6.89471236892197));
#45112=CARTESIAN_POINT('Ctrl Pts',(-25.9361777866325,25.7436554958658,6.91876137477343));
#45113=CARTESIAN_POINT('Ctrl Pts',(-26.1415302250007,25.4663429388757,6.94057118969712));
#45114=CARTESIAN_POINT('Ctrl Pts',(-26.1428550462322,25.4645499834979,6.94071197410278));
#45115=CARTESIAN_POINT('Ctrl Pts',(-26.1518004967781,25.4524172806119,6.94166310765567));
#45116=CARTESIAN_POINT('Ctrl Pts',(-26.1593612614233,25.4420332262551,6.94246961851545));
#45117=CARTESIAN_POINT('Ctrl Pts',(-26.1689670733808,25.4286733420745,6.94349734554793));
#45118=CARTESIAN_POINT('Ctrl Pts',(-26.1710693441006,25.4257390893167,6.94372245854666));
#45119=CARTESIAN_POINT('Ctrl Pts',(-26.1744105776562,25.4210589608274,6.94408053723123));
#45120=CARTESIAN_POINT('Ctrl Pts',(-26.1756527304827,25.419315382895,6.9442137238687));
#45121=CARTESIAN_POINT('Ctrl Pts',(-26.1779650394948,25.4160628010253,6.94446177571425));
#45122=CARTESIAN_POINT('Ctrl Pts',(-26.1790356264383,25.4145541236063,6.9445766705065));
#45123=CARTESIAN_POINT('Ctrl Pts',(-26.1814492720996,25.4111465870285,6.94483581116415));
#45124=CARTESIAN_POINT('Ctrl Pts',(-26.1827915719226,25.4092471991568,6.94498000399539));
#45125=CARTESIAN_POINT('Ctrl Pts',(-26.1867608858833,25.4036175999895,6.94540663040506));
#45126=CARTESIAN_POINT('Ctrl Pts',(-26.1893820503869,25.3998832413927,6.94568866050688));
#45127=CARTESIAN_POINT('Ctrl Pts',(-26.210071087473,25.370274168698,6.94791726924342));
#45128=CARTESIAN_POINT('Ctrl Pts',(-26.2277667503829,25.3441397354224,6.94983874111391));
#45129=CARTESIAN_POINT('Ctrl Pts',(-26.2939536140636,25.2432275087554,6.95710271254078));
#45130=CARTESIAN_POINT('Ctrl Pts',(-26.3397230739466,25.1667044492955,6.9622906748552));
#45131=CARTESIAN_POINT('Ctrl Pts',(-26.5144681800362,24.8449615614837,6.98322986035408));
#45132=CARTESIAN_POINT('Ctrl Pts',(-26.6147389965487,24.5855209979157,6.99821158344184));
#45133=CARTESIAN_POINT('Ctrl Pts',(-26.6850500880035,24.2982581096271,7.01532438669526));
#45134=CARTESIAN_POINT('Ctrl Pts',(-26.6893424577081,24.2800350214749,7.01641158962033));
#45135=CARTESIAN_POINT('Ctrl Pts',(-26.7144923959636,24.1689327230057,7.0230526277392));
#45136=CARTESIAN_POINT('Ctrl Pts',(-26.7313834253881,24.0752121592788,7.02871010949545));
#45137=CARTESIAN_POINT('Ctrl Pts',(-26.7454765203158,23.9706893597865,7.03513016223719));
#45138=CARTESIAN_POINT('Ctrl Pts',(-26.7468027496861,23.9604843733073,7.03575811191759));
#45139=CARTESIAN_POINT('Ctrl Pts',(-26.7485924349922,23.946177353831,7.03664011644885));
#45140=CARTESIAN_POINT('Ctrl Pts',(-26.7490969311021,23.9420804402595,7.03689287292832));
#45141=CARTESIAN_POINT('Ctrl Pts',(-26.7500059797628,23.9345794569039,7.03735599040975));
#45142=CARTESIAN_POINT('Ctrl Pts',(-26.7504129754195,23.9311756842417,7.03756627389787));
#45143=CARTESIAN_POINT('Ctrl Pts',(-26.7511833413595,23.9246446073635,7.03797001547591));
#45144=CARTESIAN_POINT('Ctrl Pts',(-26.7515475614274,23.9215174062543,7.03816344641693));
#45145=CARTESIAN_POINT('Ctrl Pts',(-26.7522983683849,23.9149877078112,7.03856757229151));
#45146=CARTESIAN_POINT('Ctrl Pts',(-26.7526841156237,23.9115851195843,7.03877829351757));
#45147=CARTESIAN_POINT('Ctrl Pts',(-26.753579195574,23.9035757950988,7.0392746255987));
#45148=CARTESIAN_POINT('Ctrl Pts',(-26.754084014079,23.8989685710524,7.03956037876169));
#45149=CARTESIAN_POINT('Ctrl Pts',(-26.7553852946594,23.8868510656411,7.04031259731485));
#45150=CARTESIAN_POINT('Ctrl Pts',(-26.756165294774,23.8793390784422,7.04077958172939));
#45151=CARTESIAN_POINT('Ctrl Pts',(-26.7677055367155,23.7642615450507,7.04794372449195));
#45152=CARTESIAN_POINT('Ctrl Pts',(-26.7730720124202,23.6562378930516,7.05481039927442));
#45153=CARTESIAN_POINT('Ctrl Pts',(-26.7730018526427,23.548160445141,7.06183203780204));
#45154=CARTESIAN_POINT('Ctrl Pts',(-26.7730018552423,23.5481644535157,7.06183177738368));
#45155=CARTESIAN_POINT('Ctrl Pts',(-26.772791063168,23.2228270107721,7.08296847867985));
#45156=CARTESIAN_POINT('Ctrl Pts',(-26.7233244541257,22.8994492477813,7.10558782499766));
#45157=CARTESIAN_POINT('Ctrl Pts',(-26.6058433168695,22.5235175808366,7.13146215824044));
#45158=CARTESIAN_POINT('Ctrl Pts',(-26.5833039843811,22.4587305605738,7.13589430784861));
#45159=CARTESIAN_POINT('Ctrl Pts',(-26.5547643434763,22.3844276793157,7.14090695062496));
#45160=CARTESIAN_POINT('Ctrl Pts',(-26.5507633807697,22.3741685778357,7.14159746206679));
#45161=CARTESIAN_POINT('Ctrl Pts',(-26.5454944464049,22.3608601085036,7.14249095649197));
#45162=CARTESIAN_POINT('Ctrl Pts',(-26.5442743236775,22.3577920613448,7.1426967800971));
#45163=CARTESIAN_POINT('Ctrl Pts',(-26.542288632768,22.3528212230282,7.14302999406615));
#45164=CARTESIAN_POINT('Ctrl Pts',(-26.5415259632994,22.3509172880979,7.14315755990102));
#45165=CARTESIAN_POINT('Ctrl Pts',(-26.5400583018947,22.3472635134997,7.14340224596881));
#45166=CARTESIAN_POINT('Ctrl Pts',(-26.5393535931335,22.3455135699529,7.14351938263826));
#45167=CARTESIAN_POINT('Ctrl Pts',(-26.5377296418131,22.3414911457455,7.14378851167677));
#45168=CARTESIAN_POINT('Ctrl Pts',(-26.5368093404816,22.3392190888751,7.1439404393934));
#45169=CARTESIAN_POINT('Ctrl Pts',(-26.5338806648122,22.3320123623605,7.14442206177389));
#45170=CARTESIAN_POINT('Ctrl Pts',(-26.531862632428,22.3270815889893,7.14475117155195));
#45171=CARTESIAN_POINT('Ctrl Pts',(-26.5145794557455,22.2851495461781,7.14754664845251));
#45172=CARTESIAN_POINT('Ctrl Pts',(-26.4986375841876,22.2484285731391,7.14997267212597));
#45173=CARTESIAN_POINT('Ctrl Pts',(-26.477412891756,22.2019303861763,7.15302804538257));
#45174=CARTESIAN_POINT('Ctrl Pts',(-26.472758922335,22.1918723254186,7.15368795081659));
#45175=CARTESIAN_POINT('Ctrl Pts',(-26.4622496334423,22.1694638987316,7.15515634396711));
#45176=CARTESIAN_POINT('Ctrl Pts',(-26.4563674165113,22.1571263144952,7.15596356984728));
#45177=CARTESIAN_POINT('Ctrl Pts',(-26.4181884256739,22.0783424096899,7.16111262405508));
#45178=CARTESIAN_POINT('Ctrl Pts',(-26.3836914538359,22.0129819421022,7.16535885502875));
#45179=CARTESIAN_POINT('Ctrl Pts',(-26.2318796180292,21.7478525818066,7.18270585633182));
#45180=CARTESIAN_POINT('Ctrl Pts',(-26.095449781197,21.5598393436681,7.19535458264382));
#45181=CARTESIAN_POINT('Ctrl Pts',(-25.8945273563607,21.3377663294674,7.21251886685697));
#45182=CARTESIAN_POINT('Ctrl Pts',(-25.8474388254048,21.2889135564165,7.21645180040281));
#45183=CARTESIAN_POINT('Ctrl Pts',(-25.7632003281092,21.2068670416785,7.22337497614159));
#45184=CARTESIAN_POINT('Ctrl Pts',(-25.7267570650453,21.1729807499142,7.22633608657135));
#45185=CARTESIAN_POINT('Ctrl Pts',(-25.6685523426869,21.1213203891957,7.23102338678131));
#45186=CARTESIAN_POINT('Ctrl Pts',(-25.647317355091,21.1029633187814,7.23272506672825));
#45187=CARTESIAN_POINT('Ctrl Pts',(-25.6207328879937,21.0805818395191,7.23484624173202));
#45188=CARTESIAN_POINT('Ctrl Pts',(-25.6156066298289,21.0762932187978,7.23525484887082));
#45189=CARTESIAN_POINT('Ctrl Pts',(-25.6079863099647,21.069958261286,7.23586165279084));
#45190=CARTESIAN_POINT('Ctrl Pts',(-25.6055024336119,21.0678996537572,7.23605934887651));
#45191=CARTESIAN_POINT('Ctrl Pts',(-25.6004717592207,21.0637430164268,7.23645956084057));
#45192=CARTESIAN_POINT('Ctrl Pts',(-25.5979248220529,21.0616451617776,7.23666208349603));
#45193=CARTESIAN_POINT('Ctrl Pts',(-25.59244772227,21.0571478990857,7.23709739529362));
#45194=CARTESIAN_POINT('Ctrl Pts',(-25.5895165454002,21.0547497391184,7.23733023462969));
#45195=CARTESIAN_POINT('Ctrl Pts',(-25.5816320169285,21.0483221326459,7.2379562114585));
#45196=CARTESIAN_POINT('Ctrl Pts',(-25.5766709246679,21.044302246794,7.23834973459933));
#45197=CARTESIAN_POINT('Ctrl Pts',(-25.5549491596986,21.0268081659813,7.24007124003913));
#45198=CARTESIAN_POINT('Ctrl Pts',(-25.5380661127394,21.013487432581,7.24140536910811));
#45199=CARTESIAN_POINT('Ctrl Pts',(-25.5107542909213,20.9923784572214,7.24355778964545));
#45200=CARTESIAN_POINT('Ctrl Pts',(-25.5004092563132,20.9844825361192,7.2443717561494));
#45201=CARTESIAN_POINT('Ctrl Pts',(-25.4853131159871,20.9731043421235,7.24555770633285));
#45202=CARTESIAN_POINT('Ctrl Pts',(-25.4805997451226,20.9695720224568,7.24592772921284));
#45203=CARTESIAN_POINT('Ctrl Pts',(-25.4701573427388,20.9617908352938,7.24674694579245));
#45204=CARTESIAN_POINT('Ctrl Pts',(-25.464423847832,20.9575480347713,7.24719637102217));
#45205=CARTESIAN_POINT('Ctrl Pts',(-25.457192620297,20.9522339691496,7.24776273567675));
#45206=CARTESIAN_POINT('Ctrl Pts',(-25.4557079568299,20.9511448818179,7.24787899318039));
#45207=CARTESIAN_POINT('Ctrl Pts',(-25.4486138848626,20.9459503111773,7.24843438286161));
#45208=CARTESIAN_POINT('Ctrl Pts',(-25.4429921695411,20.9418617356086,7.24887415666291));
#45209=CARTESIAN_POINT('Ctrl Pts',(-25.4334327576054,20.9349565182575,7.24962138789371));
#45210=CARTESIAN_POINT('Ctrl Pts',(-25.4295018439579,20.9321304904,7.24992849057835));
#45211=CARTESIAN_POINT('Ctrl Pts',(-25.4223009325626,20.926978155672,7.25049076194866));
#45212=CARTESIAN_POINT('Ctrl Pts',(-25.4190329236948,20.9246490747093,7.25074582656327));
#45213=CARTESIAN_POINT('Ctrl Pts',(-25.411653155878,20.9194103373574,7.25132155735793));
#45214=CARTESIAN_POINT('Ctrl Pts',(-25.4075389151891,20.9165042095412,7.25164235287342));
#45215=CARTESIAN_POINT('Ctrl Pts',(-25.3891493270713,20.9035790904507,7.25307544528895));
#45216=CARTESIAN_POINT('Ctrl Pts',(-25.374799809308,20.8936665756671,7.25419160631994));
#45217=CARTESIAN_POINT('Ctrl Pts',(-25.2473073184995,20.8071161352162,7.26409023163786));
#45218=CARTESIAN_POINT('Ctrl Pts',(-25.1294890483084,20.7376386628723,7.27312078295033));
#45219=CARTESIAN_POINT('Ctrl Pts',(-24.9216566857051,20.6322635678398,7.28876505733926));
#45220=CARTESIAN_POINT('Ctrl Pts',(-24.833773279846,20.5925536525158,7.29529729395809));
#45221=CARTESIAN_POINT('Ctrl Pts',(-24.5747085348605,20.4892195492738,7.31416980431325));
#45222=CARTESIAN_POINT('Ctrl Pts',(-24.3997119985493,20.4361125219717,7.32646452255243));
#45223=CARTESIAN_POINT('Ctrl Pts',(-24.2055906109272,20.3947965654028,7.33901815918339));
#45224=CARTESIAN_POINT('Ctrl Pts',(-24.1900148726184,20.3916017872667,7.34001787640688));
#45225=CARTESIAN_POINT('Ctrl Pts',(-24.1707338180533,20.3877954773254,7.34124555817823));
#45226=CARTESIAN_POINT('Ctrl Pts',(-24.1670505963051,20.3870750476945,7.34147963608449));
#45227=CARTESIAN_POINT('Ctrl Pts',(-24.1612535476739,20.385951668715,7.34184734593042));
#45228=CARTESIAN_POINT('Ctrl Pts',(-24.1591405762026,20.3855444026088,7.34198122514609));
#45229=CARTESIAN_POINT('Ctrl Pts',(-24.1551939944578,20.3847878149035,7.34223100530482));
#45230=CARTESIAN_POINT('Ctrl Pts',(-24.1533605008131,20.3844379723382,7.34234693544741));
#45231=CARTESIAN_POINT('Ctrl Pts',(-24.1492481948478,20.3836570196673,7.34260670222978));
#45232=CARTESIAN_POINT('Ctrl Pts',(-24.1469692255103,20.38322677735,7.34275048826914));
#45233=CARTESIAN_POINT('Ctrl Pts',(-24.1411841798565,20.382141095555,7.34311504917113));
#45234=CARTESIAN_POINT('Ctrl Pts',(-24.1376774658678,20.3814890139183,7.34333563160708));
#45235=CARTESIAN_POINT('Ctrl Pts',(-24.1184656232715,20.3779495145529,7.34454194124999));
#45236=CARTESIAN_POINT('Ctrl Pts',(-24.1027399208908,20.3751729642539,7.34552141526681));
#45237=CARTESIAN_POINT('Ctrl Pts',(-23.8016124003484,20.3243105198888,7.36413665936903));
#45238=CARTESIAN_POINT('Ctrl Pts',(-23.5109849449434,20.3147611379025,7.37977718443123));
#45239=CARTESIAN_POINT('Ctrl Pts',(-23.1198590570928,20.354690379954,7.40189722846873));
#45240=CARTESIAN_POINT('Ctrl Pts',(-23.0173415586127,20.3701802405233,7.40778604784257));
#45241=CARTESIAN_POINT('Ctrl Pts',(-22.8457207861161,20.4046436993957,7.41795617196829));
#45242=CARTESIAN_POINT('Ctrl Pts',(-22.7761793150165,20.4210306696376,7.42216505115728));
#45243=CARTESIAN_POINT('Ctrl Pts',(-22.6839097937773,20.4460372913502,7.42789635556053));
#45244=CARTESIAN_POINT('Ctrl Pts',(-22.6606488263648,20.4526232451091,7.42935381937877));
#45245=CARTESIAN_POINT('Ctrl Pts',(-22.6271301356691,20.4625221805971,7.43147318177829));
#45246=CARTESIAN_POINT('Ctrl Pts',(-22.616811118058,20.4656260061574,7.43212828904688));
#45247=CARTESIAN_POINT('Ctrl Pts',(-22.5984715160421,20.4712427715585,7.43329738327003));
#45248=CARTESIAN_POINT('Ctrl Pts',(-22.5904447945101,20.4737354570951,7.43381070445361));
#45249=CARTESIAN_POINT('Ctrl Pts',(-22.5784155645964,20.4775227734509,7.43458249004778));
#45250=CARTESIAN_POINT('Ctrl Pts',(-22.5744056463861,20.4787939019907,7.43484018062508));
#45251=CARTESIAN_POINT('Ctrl Pts',(-22.5673027454038,20.4810608077619,7.43529738127025));
#45252=CARTESIAN_POINT('Ctrl Pts',(-22.5642087523555,20.4820534205339,7.43549678677924));
#45253=CARTESIAN_POINT('Ctrl Pts',(-22.5580362785763,20.4840439702139,7.43589510120443));
#45254=CARTESIAN_POINT('Ctrl Pts',(-22.5549577890841,20.4850418683532,7.43609400865422));
#45255=CARTESIAN_POINT('Ctrl Pts',(-22.546626110986,20.4877564723851,7.43663301586101));
#45256=CARTESIAN_POINT('Ctrl Pts',(-22.5413758443812,20.4894820511101,7.43697340852295));
#45257=CARTESIAN_POINT('Ctrl Pts',(-22.5218651529371,20.4959501868664,7.43824110161262));
#45258=CARTESIAN_POINT('Ctrl Pts',(-22.5076336896107,20.5007789128158,7.43917125108322));
#45259=CARTESIAN_POINT('Ctrl Pts',(-22.2847731716397,20.5781377546223,7.45382458245888));
#45260=CARTESIAN_POINT('Ctrl Pts',(-22.0841519471624,20.6718124009388,7.46828502425969));
#45261=CARTESIAN_POINT('Ctrl Pts',(-21.7916788128761,20.846928895444,7.49121324581711));
#45262=CARTESIAN_POINT('Ctrl Pts',(-21.6921713746734,20.9143325966398,7.49937534582747));
#45263=CARTESIAN_POINT('Ctrl Pts',(-21.5199618668321,21.0455893910299,7.51397777405507));
#45264=CARTESIAN_POINT('Ctrl Pts',(-21.4459209391825,21.1074654745548,7.52043227576709));
#45265=CARTESIAN_POINT('Ctrl Pts',(-21.3444563501271,21.2003018666075,7.52942208454465));
#45266=CARTESIAN_POINT('Ctrl Pts',(-21.3146815527309,21.2286092204901,7.53207905586681));
#45267=CARTESIAN_POINT('Ctrl Pts',(-21.2666815142398,21.27602358869,7.53638221234977));
#45268=CARTESIAN_POINT('Ctrl Pts',(-21.2481360782834,21.2947982931931,7.53804986163973));
#45269=CARTESIAN_POINT('Ctrl Pts',(-21.2267962651321,21.3169393968376,7.53997245828482));
#45270=CARTESIAN_POINT('Ctrl Pts',(-21.2237762594394,21.3200855567527,7.54024463073137));
#45271=CARTESIAN_POINT('Ctrl Pts',(-21.219184523971,21.324888579178,7.54065857141966));
#45272=CARTESIAN_POINT('Ctrl Pts',(-21.2176081689569,21.3265409823117,7.54080069982033));
#45273=CARTESIAN_POINT('Ctrl Pts',(-21.2147480317616,21.3295454889857,7.54105861411945));
#45274=CARTESIAN_POINT('Ctrl Pts',(-21.21346367092,21.3308970263831,7.54117444528726));
#45275=CARTESIAN_POINT('Ctrl Pts',(-21.2106803695851,21.3338309987643,7.54142548840966));
#45276=CARTESIAN_POINT('Ctrl Pts',(-21.2091818655203,21.3354138356717,7.5415606661751));
#45277=CARTESIAN_POINT('Ctrl Pts',(-21.2050915306801,21.3397431554395,7.5419297035508));
#45278=CARTESIAN_POINT('Ctrl Pts',(-21.2025029092365,21.3424926865608,7.54216331358256));
#45279=CARTESIAN_POINT('Ctrl Pts',(-21.1900125993753,21.3558062086021,7.54329082889341));
#45280=CARTESIAN_POINT('Ctrl Pts',(-21.1801771418345,21.3664325143754,7.54417968625659));
#45281=CARTESIAN_POINT('Ctrl Pts',(-21.1693541032826,21.3782850586343,7.54515939428888));
#45282=CARTESIAN_POINT('Ctrl Pts',(-21.1682956349509,21.379445913753,7.54525522460535));
#45283=CARTESIAN_POINT('Ctrl Pts',(-20.9483956034279,21.6209715871171,7.56516794370171));
#45284=CARTESIAN_POINT('Ctrl Pts',(-20.7671362964794,21.8931064338559,7.58248384892978));
#45285=CARTESIAN_POINT('Ctrl Pts',(-20.5842078031875,22.285240926007,7.60703626188439));
#45286=CARTESIAN_POINT('Ctrl Pts',(-20.543664861701,22.3848756432854,7.61322765608586));
#45287=CARTESIAN_POINT('Ctrl Pts',(-20.4934454090403,22.5284700547291,7.62221428672086));
#45288=CARTESIAN_POINT('Ctrl Pts',(-20.4795898239999,22.5708958749271,7.62487657768816));
#45289=CARTESIAN_POINT('Ctrl Pts',(-20.4616778351887,22.6298650736036,7.62859296289825));
#45290=CARTESIAN_POINT('Ctrl Pts',(-20.4568644743225,22.6461745271151,7.62962248085157));
#45291=CARTESIAN_POINT('Ctrl Pts',(-20.4498938562526,22.6705011146268,7.63116082903461));
#45292=CARTESIAN_POINT('Ctrl Pts',(-20.4476380878365,22.6784899017511,7.63166645857372));
#45293=CARTESIAN_POINT('Ctrl Pts',(-20.4435915405834,22.6930353799391,7.63258791464277));
#45294=CARTESIAN_POINT('Ctrl Pts',(-20.4417905856519,22.6995892094318,7.63300340820769));
#45295=CARTESIAN_POINT('Ctrl Pts',(-20.4390007828868,22.7098687049991,7.63365559798318));
#45296=CARTESIAN_POINT('Ctrl Pts',(-20.4379978567359,22.7135905577625,7.63389183603242));
#45297=CARTESIAN_POINT('Ctrl Pts',(-20.4362230810709,22.7202240883364,7.63431307355856));
#45298=CARTESIAN_POINT('Ctrl Pts',(-20.4354486306673,22.7231350707605,7.63449798828024));
#45299=CARTESIAN_POINT('Ctrl Pts',(-20.433816575521,22.7293043933419,7.63489001966726));
#45300=CARTESIAN_POINT('Ctrl Pts',(-20.4329599975829,22.7325629992737,7.63509716942028));
#45301=CARTESIAN_POINT('Ctrl Pts',(-20.4305440606702,22.74181271121,7.63568540630311));
#45302=CARTESIAN_POINT('Ctrl Pts',(-20.4289968585103,22.7478069514308,7.63606688714573));
#45303=CARTESIAN_POINT('Ctrl Pts',(-20.4225564733642,22.7730590311039,7.63767515155898));
#45304=CARTESIAN_POINT('Ctrl Pts',(-20.4178242567538,22.7923571269514,7.63890713229311));
#45305=CARTESIAN_POINT('Ctrl Pts',(-20.3380229966455,23.1313096037672,7.66060010914705));
#45306=CARTESIAN_POINT('Ctrl Pts',(-20.3120797453052,23.4604804535238,7.68281343840332));
#45307=CARTESIAN_POINT('Ctrl Pts',(-20.3486970482049,23.9559671016107,7.71635231250167));
#45308=CARTESIAN_POINT('Ctrl Pts',(-20.3743129427217,24.1229529347272,7.72760977071262));
#45309=CARTESIAN_POINT('Ctrl Pts',(-20.4142074268507,24.2927967300776,7.73853713635104));
#45310=CARTESIAN_POINT('Ctrl Pts',(-20.415540520058,24.2984045159161,7.73889731485976));
#45311=CARTESIAN_POINT('Ctrl Pts',(-20.4174872540215,24.3064970871508,7.73941616979652));
#45312=CARTESIAN_POINT('Ctrl Pts',(-20.4180888110738,24.3089847242288,7.73957553927677));
#45313=CARTESIAN_POINT('Ctrl Pts',(-20.4191413695172,24.3133148165575,7.73985272350553));
#45314=CARTESIAN_POINT('Ctrl Pts',(-20.4195910347076,24.3151575923728,7.73997061606172));
#45315=CARTESIAN_POINT('Ctrl Pts',(-20.4204654446169,24.3187273294728,7.74019885520292));
#45316=CARTESIAN_POINT('Ctrl Pts',(-20.4208899907689,24.3204543317108,7.74030921312419));
#45317=CARTESIAN_POINT('Ctrl Pts',(-20.4219080118957,24.3245807808724,7.74057275327015));
#45318=CARTESIAN_POINT('Ctrl Pts',(-20.422502819285,24.3269799025576,7.74072585784133));
#45319=CARTESIAN_POINT('Ctrl Pts',(-20.4243130952135,24.3342457486364,7.74118919101472));
#45320=CARTESIAN_POINT('Ctrl Pts',(-20.425537174053,24.3391103511272,7.74149892310265));
#45321=CARTESIAN_POINT('Ctrl Pts',(-20.430037727319,24.3568211246066,7.74262490583368));
#45322=CARTESIAN_POINT('Ctrl Pts',(-20.4333821585991,24.3696501225706,7.74343731524509));
#45323=CARTESIAN_POINT('Ctrl Pts',(-20.5206392588227,24.696096208699,7.76403648510837));
#45324=CARTESIAN_POINT('Ctrl Pts',(-20.6513971891129,24.9953256916768,7.78133300032628));
#45325=CARTESIAN_POINT('Ctrl Pts',(-20.9077990984401,25.401685288219,7.80859403049803));
#45326=CARTESIAN_POINT('Ctrl Pts',(-21.0003140821045,25.5271611465319,7.81762297153462));
#45327=CARTESIAN_POINT('Ctrl Pts',(-21.1114546516642,25.6570547772757,7.82794708308797));
#45328=CARTESIAN_POINT('Ctrl Pts',(-21.1214657322099,25.6685880744924,7.82887270982357));
#45329=CARTESIAN_POINT('Ctrl Pts',(-21.1366265325978,25.6858053675442,7.83026825037349));
#45330=CARTESIAN_POINT('Ctrl Pts',(-21.141715280497,25.691542957167,7.83073562810581));
#45331=CARTESIAN_POINT('Ctrl Pts',(-21.1499446739746,25.7007551908365,7.83148982122015));
#45332=CARTESIAN_POINT('Ctrl Pts',(-21.1530725200089,25.7042412712239,7.8317760987448));
#45333=CARTESIAN_POINT('Ctrl Pts',(-21.1590697498251,25.7108961257881,7.83232428373989));
#45334=CARTESIAN_POINT('Ctrl Pts',(-21.1619378630086,25.7140660356886,7.83258613724012));
#45335=CARTESIAN_POINT('Ctrl Pts',(-21.1670376625938,25.7196799685721,7.83305119489872));
#45336=CARTESIAN_POINT('Ctrl Pts',(-21.1692668270736,25.7221262827303,7.83325429180324));
#45337=CARTESIAN_POINT('Ctrl Pts',(-21.1736733537322,25.7269471250379,7.83365540646793));
#45338=CARTESIAN_POINT('Ctrl Pts',(-21.1758505164851,25.7293218311563,7.83385341560884));
#45339=CARTESIAN_POINT('Ctrl Pts',(-21.1811022068799,25.7350328145702,7.83433063583144));
#45340=CARTESIAN_POINT('Ctrl Pts',(-21.1841802199276,25.7383658654079,7.83460999578571));
#45341=CARTESIAN_POINT('Ctrl Pts',(-21.1936539554178,25.7485812114403,7.83546880164589));
#45342=CARTESIAN_POINT('Ctrl Pts',(-21.2000727010021,25.7554420007215,7.83604923557149));
#45343=CARTESIAN_POINT('Ctrl Pts',(-21.2238356547185,25.7806198587517,7.83819289763715));
#45344=CARTESIAN_POINT('Ctrl Pts',(-21.2413643926754,25.7987607932295,7.83976410579842));
#45345=CARTESIAN_POINT('Ctrl Pts',(-21.2633442531961,25.8209802660862,7.84172241657613));
#45346=CARTESIAN_POINT('Ctrl Pts',(-21.2675966128527,25.825254921447,7.8421007416229));
#45347=CARTESIAN_POINT('Ctrl Pts',(-21.2767155100571,25.8343703241402,7.84291088658294));
#45348=CARTESIAN_POINT('Ctrl Pts',(-21.2815855604998,25.8392075009237,7.84334286021126));
#45349=CARTESIAN_POINT('Ctrl Pts',(-21.2875879278709,25.8451313772457,7.84387442701901));
#45350=CARTESIAN_POINT('Ctrl Pts',(-21.2887056619746,25.8462328846594,7.84397337725193));
#45351=CARTESIAN_POINT('Ctrl Pts',(-21.2941561469413,25.8515964005401,7.84445572127461));
#45352=CARTESIAN_POINT('Ctrl Pts',(-21.2985001211947,25.8558469411617,7.84483960903609));
#45353=CARTESIAN_POINT('Ctrl Pts',(-21.3097739136547,25.8668159962973,7.84583452858798));
#45354=CARTESIAN_POINT('Ctrl Pts',(-21.3167219002058,25.8735156761522,7.84644635835668));
#45355=CARTESIAN_POINT('Ctrl Pts',(-21.32657766435,25.8829341413863,7.84731237856716));
#45356=CARTESIAN_POINT('Ctrl Pts',(-21.3294605925896,25.8856789533219,7.84756547620041));
#45357=CARTESIAN_POINT('Ctrl Pts',(-21.336110999795,25.8919873014671,7.84814881498995));
#45358=CARTESIAN_POINT('Ctrl Pts',(-21.3398820022834,25.8955470926088,7.84847921021904));
#45359=CARTESIAN_POINT('Ctrl Pts',(-21.3609714408584,25.9153592813113,7.8503248592468));
#45360=CARTESIAN_POINT('Ctrl Pts',(-21.3784601787074,25.9314286193731,7.85184753991441));
#45361=CARTESIAN_POINT('Ctrl Pts',(-21.5651346063039,26.0991850481535,7.86801869267713));
#45362=CARTESIAN_POINT('Ctrl Pts',(-21.7497122490894,26.2327469140146,7.88337345929642));
#45363=CARTESIAN_POINT('Ctrl Pts',(-21.9889929044795,26.3699965076479,7.90203741202108));
#45364=CARTESIAN_POINT('Ctrl Pts',(-22.0317618329255,26.3932566857474,7.90532646861328));
#45365=CARTESIAN_POINT('Ctrl Pts',(-22.0750360380806,26.4155367862613,7.90859913775027));
#45366=CARTESIAN_POINT('Origin',(-23.5502525316942,23.5502525316942,-77.3107734492734));
#45367=CARTESIAN_POINT('',(-22.0750360149249,26.4155367743394,9.40666775021339));
#45368=CARTESIAN_POINT('',(-22.0750360476606,26.4155367911937,9.15896072794325));
#45369=CARTESIAN_POINT('',(-22.0750360153461,26.4155367745563,-77.3107734492734));
#45370=CARTESIAN_POINT('',(-26.7730012608198,23.553114597239,8.56023136266877));
#45371=CARTESIAN_POINT('Ctrl Pts',(-22.0750360149249,26.4155367743394,9.40666775021339));
#45372=CARTESIAN_POINT('Ctrl Pts',(-22.0693300256039,26.4125989961025,9.4062620900943));
#45373=CARTESIAN_POINT('Ctrl Pts',(-22.0636327609311,26.409644147122,9.40585583565952));
#45374=CARTESIAN_POINT('Ctrl Pts',(-21.9435252406745,26.346895161247,9.39726559129291));
#45375=CARTESIAN_POINT('Ctrl Pts',(-21.8328148432258,26.2803044304993,9.38884597643277));
#45376=CARTESIAN_POINT('Ctrl Pts',(-21.5324258522311,26.074108930731,9.36460508212239));
#45377=CARTESIAN_POINT('Ctrl Pts',(-21.3536239453862,25.920123866776,9.34841892696947));
#45378=CARTESIAN_POINT('Ctrl Pts',(-21.1296348953135,25.6799028791358,9.32666615536534));
#45379=CARTESIAN_POINT('Ctrl Pts',(-21.0690666933332,25.609019407015,9.32060872175227));
#45380=CARTESIAN_POINT('Ctrl Pts',(-21.0076685433264,25.5305116053166,9.31436033330049));
#45381=CARTESIAN_POINT('Ctrl Pts',(-21.0037021700256,25.5254083720678,9.31395617429862));
#45382=CARTESIAN_POINT('Ctrl Pts',(-20.9982314939797,25.5183257939267,9.31339806739935));
#45383=CARTESIAN_POINT('Ctrl Pts',(-20.996714123185,25.5163566334198,9.31324319709865));
#45384=CARTESIAN_POINT('Ctrl Pts',(-20.9941128869307,25.5129728008574,9.31297758244524));
#45385=CARTESIAN_POINT('Ctrl Pts',(-20.9930279167191,25.5115589858508,9.3128667592348));
#45386=CARTESIAN_POINT('Ctrl Pts',(-20.9909073220547,25.5087909068412,9.31265008409845));
#45387=CARTESIAN_POINT('Ctrl Pts',(-20.9898716019989,25.5074367243268,9.31254422556778));
#45388=CARTESIAN_POINT('Ctrl Pts',(-20.9877256744779,25.5046263499756,9.31232482730887));
#45389=CARTESIAN_POINT('Ctrl Pts',(-20.9866156314956,25.5031700311086,9.31221129930498));
#45390=CARTESIAN_POINT('Ctrl Pts',(-20.9830523757719,25.4984869508863,9.31184674776189));
#45391=CARTESIAN_POINT('Ctrl Pts',(-20.9806039966487,25.4952564904199,9.31159606707401));
#45392=CARTESIAN_POINT('Ctrl Pts',(-20.965830058176,25.4756867505273,9.31008220323844));
#45393=CARTESIAN_POINT('Ctrl Pts',(-20.9536539192366,25.4592344985968,9.30882940426677));
#45394=CARTESIAN_POINT('Ctrl Pts',(-20.9176690953964,25.4096308563872,9.30510768633075));
#45395=CARTESIAN_POINT('Ctrl Pts',(-20.8943317034875,25.376140863071,9.30266811575634));
#45396=CARTESIAN_POINT('Ctrl Pts',(-20.8306241714621,25.2809111451613,9.29590641296271));
#45397=CARTESIAN_POINT('Ctrl Pts',(-20.7917266950463,25.2182136249794,9.29165568680662));
#45398=CARTESIAN_POINT('Ctrl Pts',(-20.6633507077381,24.9944941470433,9.2769814377123));
#45399=CARTESIAN_POINT('Ctrl Pts',(-20.5855480221316,24.8271892071836,9.26685123065548));
#45400=CARTESIAN_POINT('Ctrl Pts',(-20.4575583560361,24.4761366516479,9.24576355663737));
#45401=CARTESIAN_POINT('Ctrl Pts',(-20.4084912742498,24.2927743407578,9.23482534984744));
#45402=CARTESIAN_POINT('Ctrl Pts',(-20.3736498714154,24.0938244850829,9.22255146402142));
#45403=CARTESIAN_POINT('Ctrl Pts',(-20.371558099717,24.0814555352083,9.22178688164962));
#45404=CARTESIAN_POINT('Ctrl Pts',(-20.3687963068003,24.0645239705988,9.2207381149868));
#45405=CARTESIAN_POINT('Ctrl Pts',(-20.3680637649673,24.0599715487491,9.22045591918552));
#45406=CARTESIAN_POINT('Ctrl Pts',(-20.3668328530604,24.0522158981095,9.21997479503461));
#45407=CARTESIAN_POINT('Ctrl Pts',(-20.3663295400452,24.049013451043,9.21977602394863));
#45408=CARTESIAN_POINT('Ctrl Pts',(-20.36536478065,24.0428139704086,9.21939102364812));
#45409=CARTESIAN_POINT('Ctrl Pts',(-20.3649027304998,24.0398170336681,9.21920481386912));
#45410=CARTESIAN_POINT('Ctrl Pts',(-20.3638154301726,24.0326979109214,9.21876225364762));
#45411=CARTESIAN_POINT('Ctrl Pts',(-20.3631939494743,24.0285751624877,9.21850578383988));
#45412=CARTESIAN_POINT('Ctrl Pts',(-20.3613812182265,24.0163895687537,9.21774720111604));
#45413=CARTESIAN_POINT('Ctrl Pts',(-20.3602125585587,24.0083234421623,9.21724437240861));
#45414=CARTESIAN_POINT('Ctrl Pts',(-20.3514109870511,23.9459071077258,9.2133479698746));
#45415=CARTESIAN_POINT('Ctrl Pts',(-20.3451373821073,23.89137721419,9.20991157343925));
#45416=CARTESIAN_POINT('Ctrl Pts',(-20.3285629176543,23.7056507099242,9.19808767401274));
#45417=CARTESIAN_POINT('Ctrl Pts',(-20.3249059031371,23.5740076506254,9.18949828178691));
#45418=CARTESIAN_POINT('Ctrl Pts',(-20.335614439619,23.2538394464317,9.16816640502373));
#45419=CARTESIAN_POINT('Ctrl Pts',(-20.3584930227046,23.0660789795015,9.15526830049522));
#45420=CARTESIAN_POINT('Ctrl Pts',(-20.4151134410909,22.7991967900413,9.13695481410728));
#45421=CARTESIAN_POINT('Ctrl Pts',(-20.4357677104259,22.7176853581571,9.13136919100403));
#45422=CARTESIAN_POINT('Ctrl Pts',(-20.4612775668464,22.6313472953767,9.12552111545527));
#45423=CARTESIAN_POINT('Ctrl Pts',(-20.4629842294908,22.6256295825864,9.12513415731335));
#45424=CARTESIAN_POINT('Ctrl Pts',(-20.465247116399,22.6181245074014,9.1246266968221));
#45425=CARTESIAN_POINT('Ctrl Pts',(-20.4657890208632,22.616332879659,9.12450558932912));
#45426=CARTESIAN_POINT('Ctrl Pts',(-20.4796955156024,22.570499789582,9.12140834197518));
#45427=CARTESIAN_POINT('Ctrl Pts',(-20.4940013530364,22.526746251127,9.11847289634632));
#45428=CARTESIAN_POINT('Ctrl Pts',(-20.5108916692095,22.4786052084335,9.11527833924467));
#45429=CARTESIAN_POINT('Ctrl Pts',(-20.5125538006588,22.473902747416,9.11496666862692));
#45430=CARTESIAN_POINT('Ctrl Pts',(-20.5150535622051,22.4668823955026,9.1145019558835));
#45431=CARTESIAN_POINT('Ctrl Pts',(-20.5158829355488,22.4645616040046,9.11434842634014));
#45432=CARTESIAN_POINT('Ctrl Pts',(-20.5173147031102,22.4605696208619,9.1140845079674));
#45433=CARTESIAN_POINT('Ctrl Pts',(-20.5179158167595,22.4588979763322,9.11397404251936));
#45434=CARTESIAN_POINT('Ctrl Pts',(-20.5191619956764,22.4554414398206,9.11374573372434));
#45435=CARTESIAN_POINT('Ctrl Pts',(-20.519807254317,22.453656623776,9.11362790282481));
#45436=CARTESIAN_POINT('Ctrl Pts',(-20.5210918133376,22.4501132650449,9.11339409018688));
#45437=CARTESIAN_POINT('Ctrl Pts',(-20.5217310699706,22.4483547054051,9.11327810567341));
#45438=CARTESIAN_POINT('Ctrl Pts',(-20.5238902199993,22.4424310755551,9.11288760286627));
#45439=CARTESIAN_POINT('Ctrl Pts',(-20.5254171857286,22.438268561178,9.11261350768204));
#45440=CARTESIAN_POINT('Ctrl Pts',(-20.5368118229272,22.4074038839989,9.11058332353545));
#45441=CARTESIAN_POINT('Ctrl Pts',(-20.5470247154046,22.3808292741652,9.10884759892222));
#45442=CARTESIAN_POINT('Ctrl Pts',(-20.5820941431527,22.2930673361856,9.10314533178313));
#45443=CARTESIAN_POINT('Ctrl Pts',(-20.60848047932,22.2325054818348,9.09925901855854));
#45444=CARTESIAN_POINT('Ctrl Pts',(-20.7087806914538,22.0203548928187,9.08567501500552));
#45445=CARTESIAN_POINT('Ctrl Pts',(-20.792707293267,21.8737976715654,9.07633574171811));
#45446=CARTESIAN_POINT('Ctrl Pts',(-20.9628748402892,21.6242759900253,9.05944158206174));
#45447=CARTESIAN_POINT('Ctrl Pts',(-21.0447920665079,21.5188556147609,9.05194001832127));
#45448=CARTESIAN_POINT('Ctrl Pts',(-21.1622847017217,21.3856075767023,9.04166473116141));
#45449=CARTESIAN_POINT('Ctrl Pts',(-21.1922495148485,21.3530043282206,9.03908206765125));
#45450=CARTESIAN_POINT('Ctrl Pts',(-21.2725462309406,21.2691720958402,9.0322434301737));
#45451=CARTESIAN_POINT('Ctrl Pts',(-21.3239328900941,21.2189924467901,9.02794715876865));
#45452=CARTESIAN_POINT('Ctrl Pts',(-21.3839983972756,21.1641360816232,9.0229928859103));
#45453=CARTESIAN_POINT('Ctrl Pts',(-21.3910756550575,21.1577300343084,9.02241017983554));
#45454=CARTESIAN_POINT('Ctrl Pts',(-21.4014558845418,21.1484178401541,9.02155698346243));
#45455=CARTESIAN_POINT('Ctrl Pts',(-21.4047365576394,21.1454868214699,9.02128754206462));
#45456=CARTESIAN_POINT('Ctrl Pts',(-21.4105544469587,21.1403103854906,9.02081008790857));
#45457=CARTESIAN_POINT('Ctrl Pts',(-21.4130892270996,21.1380622300754,9.02060219050962));
#45458=CARTESIAN_POINT('Ctrl Pts',(-21.4183540237514,21.1334075721226,9.02017063559648));
#45459=CARTESIAN_POINT('Ctrl Pts',(-21.4210845795764,21.1310016893307,9.01994695258616));
#45460=CARTESIAN_POINT('Ctrl Pts',(-21.4281204399331,21.1248235566051,9.01937094240777));
#45461=CARTESIAN_POINT('Ctrl Pts',(-21.4324317165647,21.1210581544547,9.01901833044802));
#45462=CARTESIAN_POINT('Ctrl Pts',(-21.4500441560077,21.105758247107,9.01757920980507));
#45463=CARTESIAN_POINT('Ctrl Pts',(-21.4634295049765,21.0943215139235,9.01648865867825));
#45464=CARTESIAN_POINT('Ctrl Pts',(-21.4976616129309,21.0655547678957,9.01370729219794));
#45465=CARTESIAN_POINT('Ctrl Pts',(-21.5186342433715,21.0483773319089,9.01201033876448));
#45466=CARTESIAN_POINT('Ctrl Pts',(-21.6035427254177,20.9806054954448,9.00516674341493));
#45467=CARTESIAN_POINT('Ctrl Pts',(-21.6691669919205,20.9321844912677,8.99993579921483));
#45468=CARTESIAN_POINT('Ctrl Pts',(-21.9118819206311,20.7669363122878,8.98079066413754));
#45469=CARTESIAN_POINT('Ctrl Pts',(-22.0985520839433,20.6651782209173,8.96639241997261));
#45470=CARTESIAN_POINT('Ctrl Pts',(-22.4317794521799,20.5241040243134,8.94193647466219));
#45471=CARTESIAN_POINT('Ctrl Pts',(-22.5736433853384,20.47538653545,8.93188904065837));
#45472=CARTESIAN_POINT('Ctrl Pts',(-22.7218603744945,20.4357867892199,8.92207143605047));
#45473=CARTESIAN_POINT('Ctrl Pts',(-22.725327123705,20.4348667612535,8.92184218289966));
#45474=CARTESIAN_POINT('Ctrl Pts',(-22.7339025768487,20.4326062706231,8.92127604076997));
#45475=CARTESIAN_POINT('Ctrl Pts',(-22.7390130760553,20.4312725695241,8.92093947971316));
#45476=CARTESIAN_POINT('Ctrl Pts',(-22.7529741535043,20.4276657436314,8.92002235152611));
#45477=CARTESIAN_POINT('Ctrl Pts',(-22.7618312377635,20.425417667412,8.91944303763402));
#45478=CARTESIAN_POINT('Ctrl Pts',(-22.7845531374309,20.4197532266932,8.91796354097226));
#45479=CARTESIAN_POINT('Ctrl Pts',(-22.7984315052796,20.4163912355797,8.91706622479146));
#45480=CARTESIAN_POINT('Ctrl Pts',(-22.81598898155,20.4122613407582,8.91593944024253));
#45481=CARTESIAN_POINT('Ctrl Pts',(-22.8196474222199,20.4114075451084,8.91570511278049));
#45482=CARTESIAN_POINT('Ctrl Pts',(-22.8254263324583,20.4100695315962,8.91533570186497));
#45483=CARTESIAN_POINT('Ctrl Pts',(-22.8275457989952,20.409581063396,8.91520037313522));
#45484=CARTESIAN_POINT('Ctrl Pts',(-22.8314831907167,20.4086778192568,8.9149492609704));
#45485=CARTESIAN_POINT('Ctrl Pts',(-22.8333009701613,20.4082624779539,8.9148334454313));
#45486=CARTESIAN_POINT('Ctrl Pts',(-22.8373511078308,20.407340766768,8.91457565739511));
#45487=CARTESIAN_POINT('Ctrl Pts',(-22.8395836402864,20.4068351987393,8.9144337320227));
#45488=CARTESIAN_POINT('Ctrl Pts',(-22.8442020414387,20.4057945106066,8.91414048872522));
#45489=CARTESIAN_POINT('Ctrl Pts',(-22.8465879853694,20.4052597260567,8.91398919023795));
#45490=CARTESIAN_POINT('Ctrl Pts',(-22.8595563643712,20.4023684951574,8.913167886954));
#45491=CARTESIAN_POINT('Ctrl Pts',(-22.8701501992939,20.4000627075052,8.91250077538682));
#45492=CARTESIAN_POINT('Ctrl Pts',(-22.9629288743122,20.3803589251436,8.90669002662913));
#45493=CARTESIAN_POINT('Ctrl Pts',(-23.0457613558124,20.3661253360119,8.90171917797257));
#45494=CARTESIAN_POINT('Ctrl Pts',(-23.2670546327331,20.3369537530503,8.88878692402686));
#45495=CARTESIAN_POINT('Ctrl Pts',(-23.4060887453021,20.3277206224911,8.88101472695495));
#45496=CARTESIAN_POINT('Ctrl Pts',(-23.8151514386645,20.3270909595107,8.85815754936258));
#45497=CARTESIAN_POINT('Ctrl Pts',(-24.0839495696946,20.3605686570519,8.84305050621779));
#45498=CARTESIAN_POINT('Ctrl Pts',(-24.3494520537814,20.4281674904296,8.82645218949149));
#45499=CARTESIAN_POINT('Ctrl Pts',(-24.3534829326035,20.4292020989398,8.82619981888059));
#45500=CARTESIAN_POINT('Ctrl Pts',(-24.3712390374454,20.4337962473421,8.82508646066624));
#45501=CARTESIAN_POINT('Ctrl Pts',(-24.3849425283699,20.4374384970469,8.82422283586093));
#45502=CARTESIAN_POINT('Ctrl Pts',(-24.4038252106915,20.4425909766921,8.82302660953199));
#45503=CARTESIAN_POINT('Ctrl Pts',(-24.4090254547232,20.4440239945641,8.82269652098761));
#45504=CARTESIAN_POINT('Ctrl Pts',(-24.4173145965464,20.446330618598,8.82216931564578));
#45505=CARTESIAN_POINT('Ctrl Pts',(-24.420405845019,20.4471958003253,8.82197247364255));
#45506=CARTESIAN_POINT('Ctrl Pts',(-24.4264256675265,20.4488903369573,8.82158869274214));
#45507=CARTESIAN_POINT('Ctrl Pts',(-24.4293543704854,20.4497192253362,8.82140176923354));
#45508=CARTESIAN_POINT('Ctrl Pts',(-24.4363699305157,20.4517155247679,8.82095349707542));
#45509=CARTESIAN_POINT('Ctrl Pts',(-24.4404556528194,20.452886871872,8.82069202012794));
#45510=CARTESIAN_POINT('Ctrl Pts',(-24.4527487607334,20.4564375498956,8.81990404059399));
#45511=CARTESIAN_POINT('Ctrl Pts',(-24.4609489632615,20.4588414311923,8.81937673591742));
#45512=CARTESIAN_POINT('Ctrl Pts',(-24.5122985095431,20.4741165407056,8.81606412278944));
#45513=CARTESIAN_POINT('Ctrl Pts',(-24.555181880308,20.4878577545529,8.81325039051559));
#45514=CARTESIAN_POINT('Ctrl Pts',(-24.6878813297448,20.5334662896443,8.80438963721416));
#45515=CARTESIAN_POINT('Ctrl Pts',(-24.7765746908378,20.5684192842294,8.7982428594651));
#45516=CARTESIAN_POINT('Ctrl Pts',(-24.9497362750173,20.6456934639883,8.7857932618309));
#45517=CARTESIAN_POINT('Ctrl Pts',(-25.0341547673249,20.6879020549993,8.77949860670387));
#45518=CARTESIAN_POINT('Ctrl Pts',(-25.1923601552144,20.7758849055145,8.7673137328769));
#45519=CARTESIAN_POINT('Ctrl Pts',(-25.2663926880752,20.8210592948337,8.76143716296441));
#45520=CARTESIAN_POINT('Ctrl Pts',(-25.4915762096681,20.9712544362521,8.74312637556821));
#45521=CARTESIAN_POINT('Ctrl Pts',(-25.6356371264473,21.0862806123738,8.73075174116724));
#45522=CARTESIAN_POINT('Ctrl Pts',(-25.7768761663417,21.2203642251367,8.71848811026165));
#45523=CARTESIAN_POINT('Ctrl Pts',(-25.7846089752406,21.2277789317789,8.71781628523167));
#45524=CARTESIAN_POINT('Ctrl Pts',(-25.7947493448923,21.237599682926,8.71693494692813));
#45525=CARTESIAN_POINT('Ctrl Pts',(-25.7971901563625,21.239971065189,8.71672278014685));
#45526=CARTESIAN_POINT('Ctrl Pts',(-25.8009639274506,21.2436491285054,8.71639471181653));
#45527=CARTESIAN_POINT('Ctrl Pts',(-25.8022995063561,21.2449530998311,8.71627859814008));
#45528=CARTESIAN_POINT('Ctrl Pts',(-25.8049689389292,21.2475638917852,8.71604650878675));
#45529=CARTESIAN_POINT('Ctrl Pts',(-25.8063027812085,21.2488707030718,8.71593053433649));
#45530=CARTESIAN_POINT('Ctrl Pts',(-25.8089213861267,21.2514407049622,8.71570284068252));
#45531=CARTESIAN_POINT('Ctrl Pts',(-25.8102062196352,21.2527038081397,8.7155911156034));
#45532=CARTESIAN_POINT('Ctrl Pts',(-25.8131135242264,21.2555667399545,8.71533829030188));
#45533=CARTESIAN_POINT('Ctrl Pts',(-25.8147353614414,21.2571672153153,8.71519724116482));
#45534=CARTESIAN_POINT('Ctrl Pts',(-25.8188380179117,21.2612244313439,8.71484040668034));
#45535=CARTESIAN_POINT('Ctrl Pts',(-25.8213165525828,21.2636834936448,8.71462480318672));
#45536=CARTESIAN_POINT('Ctrl Pts',(-25.855970368343,21.2981769842126,8.71160982936855));
#45537=CARTESIAN_POINT('Ctrl Pts',(-25.8874711995232,21.3308858581414,8.70886314859998));
#45538=CARTESIAN_POINT('Ctrl Pts',(-25.9826650230089,21.434006052176,8.70050218753649));
#45539=CARTESIAN_POINT('Ctrl Pts',(-26.0439497945611,21.5065777453247,8.69503116718976));
#45540=CARTESIAN_POINT('Ctrl Pts',(-26.1244886013955,21.6109773165457,8.68754748319553));
#45541=CARTESIAN_POINT('Ctrl Pts',(-26.1465287066999,21.6405850705771,8.68546582208182));
#45542=CARTESIAN_POINT('Ctrl Pts',(-26.1914757742143,21.7031819615139,8.68113504891112));
#45543=CARTESIAN_POINT('Ctrl Pts',(-26.2142844066333,21.7362337525186,8.67888769499534));
#45544=CARTESIAN_POINT('Ctrl Pts',(-26.3925103800117,22.0051135269178,8.66085334732086));
#45545=CARTESIAN_POINT('Ctrl Pts',(-26.5169070678735,22.2599736962512,8.64512639871806));
#45546=CARTESIAN_POINT('Ctrl Pts',(-26.6122974331258,22.5450995320368,8.62692134050195));
#45547=CARTESIAN_POINT('Ctrl Pts',(-26.6179478791951,22.562478891335,8.62581002499323));
#45548=CARTESIAN_POINT('Ctrl Pts',(-26.6252528671905,22.5856145957235,8.62432812167044));
#45549=CARTESIAN_POINT('Ctrl Pts',(-26.6270396910123,22.5913290799494,8.62396189239165));
#45550=CARTESIAN_POINT('Ctrl Pts',(-26.6297949656264,22.6002277756664,8.62339126926788));
#45551=CARTESIAN_POINT('Ctrl Pts',(-26.6307744322144,22.6034085848176,8.62318723756324));
#45552=CARTESIAN_POINT('Ctrl Pts',(-26.632720139406,22.6097622284839,8.62277955483131));
#45553=CARTESIAN_POINT('Ctrl Pts',(-26.6336864128171,22.6129350488533,8.62257590516293));
#45554=CARTESIAN_POINT('Ctrl Pts',(-26.635845510548,22.6200640531551,8.62211817647134));
#45555=CARTESIAN_POINT('Ctrl Pts',(-26.6370356258624,22.6240210454758,8.62186400901926));
#45556=CARTESIAN_POINT('Ctrl Pts',(-26.6404994314427,22.635618610807,8.62111876172893));
#45557=CARTESIAN_POINT('Ctrl Pts',(-26.6427523742123,22.6432653030972,8.6206270036299));
#45558=CARTESIAN_POINT('Ctrl Pts',(-26.6477628632152,22.6605070748685,8.61951727753619));
#45559=CARTESIAN_POINT('Ctrl Pts',(-26.6505042317609,22.6701067344287,8.61889878542121));
#45560=CARTESIAN_POINT('Ctrl Pts',(-26.6590936589302,22.7007230690444,8.61692412621599));
#45561=CARTESIAN_POINT('Ctrl Pts',(-26.6647728495127,22.7217861084657,8.61556248635779));
#45562=CARTESIAN_POINT('Ctrl Pts',(-26.6858634014066,22.8032902772804,8.61028067296137));
#45563=CARTESIAN_POINT('Ctrl Pts',(-26.6997318346485,22.8641130477225,8.60631148929673));
#45564=CARTESIAN_POINT('Ctrl Pts',(-26.7527053584887,23.1320994880918,8.58869568065027));
#45565=CARTESIAN_POINT('Ctrl Pts',(-26.7731884098208,23.3423807074104,8.57449613895324));
#45566=CARTESIAN_POINT('Ctrl Pts',(-26.7730012608198,23.553114597239,8.56023136266877));
#45567=CARTESIAN_POINT('Ctrl Pts',(-26.7730012594657,23.5531161215966,8.56023125948356));
#45568=CARTESIAN_POINT('Ctrl Pts',(-26.7728196090006,23.7575496561465,8.54639296027699));
#45569=CARTESIAN_POINT('Ctrl Pts',(-26.7531861185436,23.9615361605529,8.53256708739775));
#45570=CARTESIAN_POINT('Ctrl Pts',(-26.7132557045306,24.1679592180812,8.51935782217261));
#45571=CARTESIAN_POINT('Ctrl Pts',(-26.7121486081331,24.1736014105547,8.51899740405998));
#45572=CARTESIAN_POINT('Ctrl Pts',(-26.7104005545642,24.1823856813531,8.51843729125752));
#45573=CARTESIAN_POINT('Ctrl Pts',(-26.7097700043974,24.1855297823828,8.51823701691999));
#45574=CARTESIAN_POINT('Ctrl Pts',(-26.7087070018829,24.1907894821639,8.51790232884377));
#45575=CARTESIAN_POINT('Ctrl Pts',(-26.7082771158951,24.1929055880308,8.51776776959212));
#45576=CARTESIAN_POINT('Ctrl Pts',(-26.7074278434914,24.1970646858325,8.51750348716521));
#45577=CARTESIAN_POINT('Ctrl Pts',(-26.7070086001398,24.199107705484,8.51737375584393));
#45578=CARTESIAN_POINT('Ctrl Pts',(-26.7062083077674,24.2029884848148,8.51712749762943));
#45579=CARTESIAN_POINT('Ctrl Pts',(-26.7058276394067,24.2048263049453,8.51701095007932));
#45580=CARTESIAN_POINT('Ctrl Pts',(-26.704951768458,24.209036381538,8.51674412876978));
#45581=CARTESIAN_POINT('Ctrl Pts',(-26.7044554960813,24.2114084095304,8.51659391758523));
#45582=CARTESIAN_POINT('Ctrl Pts',(-26.7029176085045,24.218717893009,8.51613140177687));
#45583=CARTESIAN_POINT('Ctrl Pts',(-26.7018670656432,24.2236534940032,8.51581960958387));
#45584=CARTESIAN_POINT('Ctrl Pts',(-26.6938150170095,24.261051585203,8.51346084901651));
#45585=CARTESIAN_POINT('Ctrl Pts',(-26.6863233873323,24.293408095687,8.51144152933166));
#45586=CARTESIAN_POINT('Ctrl Pts',(-26.6763962668058,24.3334560034595,8.50896240638243));
#45587=CARTESIAN_POINT('Ctrl Pts',(-26.6744306793447,24.3412602656334,8.50848025050184));
#45588=CARTESIAN_POINT('Ctrl Pts',(-26.6317962774281,24.5078997838623,8.49820398927304));
#45589=CARTESIAN_POINT('Ctrl Pts',(-26.5790890788471,24.663428986897,8.48897307272299));
#45590=CARTESIAN_POINT('Ctrl Pts',(-26.5036208403333,24.8404232976196,8.47820548699661));
#45591=CARTESIAN_POINT('Ctrl Pts',(-26.4921306508403,24.8664128987262,8.47661771679408));
#45592=CARTESIAN_POINT('Ctrl Pts',(-26.4701175416513,24.9144752476664,8.47366394404807));
#45593=CARTESIAN_POINT('Ctrl Pts',(-26.4596842412649,24.9365866976639,8.47229802557481));
#45594=CARTESIAN_POINT('Ctrl Pts',(-26.4273223206903,25.0031970791608,8.46815690135125));
#45595=CARTESIAN_POINT('Ctrl Pts',(-26.404617164617,25.047309934142,8.46537837000793));
#45596=CARTESIAN_POINT('Ctrl Pts',(-26.3152669558422,25.2114762383933,8.45485317602641));
#45597=CARTESIAN_POINT('Ctrl Pts',(-26.2419975088004,25.3277430344337,8.44701098538239));
#45598=CARTESIAN_POINT('Ctrl Pts',(-26.1259809733067,25.4881438030073,8.43532242598728));
#45599=CARTESIAN_POINT('Ctrl Pts',(-26.0890394989321,25.5362937152804,8.43169187632456));
#45600=CARTESIAN_POINT('Ctrl Pts',(-26.0449155060824,25.5905613594779,8.4274442720638));
#45601=CARTESIAN_POINT('Ctrl Pts',(-26.0390373624628,25.5977274477428,8.42688015502983));
#45602=CARTESIAN_POINT('Ctrl Pts',(-26.0283436062351,25.6106501915799,8.42585697534395));
#45603=CARTESIAN_POINT('Ctrl Pts',(-26.0235386256651,25.6164155907117,8.42539834622326));
#45604=CARTESIAN_POINT('Ctrl Pts',(-26.0161206527701,25.625253312027,8.42469199003975));
#45605=CARTESIAN_POINT('Ctrl Pts',(-26.0135219366227,25.6283376279852,8.4244448486151));
#45606=CARTESIAN_POINT('Ctrl Pts',(-26.0089692228177,25.6337205292647,8.42401242361477));
#45607=CARTESIAN_POINT('Ctrl Pts',(-26.0070177704295,25.6360212690553,8.42382724496245));
#45608=CARTESIAN_POINT('Ctrl Pts',(-26.0029201503349,25.6408385868944,8.42343877255174));
#45609=CARTESIAN_POINT('Ctrl Pts',(-26.0007733344801,25.6433546067758,8.42323545215164));
#45610=CARTESIAN_POINT('Ctrl Pts',(-25.9947964162373,25.6503376211207,8.42266996248267));
#45611=CARTESIAN_POINT('Ctrl Pts',(-25.9909579615428,25.6547974208,8.42230744752332));
#45612=CARTESIAN_POINT('Ctrl Pts',(-25.9756516325742,25.6724832458901,8.42086442395779));
#45613=CARTESIAN_POINT('Ctrl Pts',(-25.9640884589165,25.685626058695,8.41977995140539));
#45614=CARTESIAN_POINT('Ctrl Pts',(-25.7714889400267,25.9009730692326,8.40180694506239));
#45615=CARTESIAN_POINT('Ctrl Pts',(-25.5657695117716,26.0795618370056,8.38377041670967));
#45616=CARTESIAN_POINT('Ctrl Pts',(-25.2774714441396,26.2721117113345,8.36031096543834));
#45617=CARTESIAN_POINT('Ctrl Pts',(-25.2133201405861,26.3117754642694,8.35520110835401));
#45618=CARTESIAN_POINT('Ctrl Pts',(-25.0723894771157,26.3922172448623,8.34427388261923));
#45619=CARTESIAN_POINT('Ctrl Pts',(-24.9952273661546,26.432216083076,8.33847120855214));
#45620=CARTESIAN_POINT('Ctrl Pts',(-24.8748410784521,26.4885687895117,8.3297793857843));
#45621=CARTESIAN_POINT('Ctrl Pts',(-24.8327273272608,26.5071928652991,8.3268040515201));
#45622=CARTESIAN_POINT('Ctrl Pts',(-24.7765973542574,26.5305904274676,8.32293719801859));
#45623=CARTESIAN_POINT('Ctrl Pts',(-24.7629288962999,26.5361781253241,8.3220031860775));
#45624=CARTESIAN_POINT('Ctrl Pts',(-24.7403665159098,26.5452211940925,8.32047450659421));
#45625=CARTESIAN_POINT('Ctrl Pts',(-24.7314949607927,26.5487312982271,8.31987673685794));
#45626=CARTESIAN_POINT('Ctrl Pts',(-24.7204165125042,26.5530577792377,8.31913450134647));
#45627=CARTESIAN_POINT('Ctrl Pts',(-24.7182242638808,26.5539111556988,8.3189878309754));
#45628=CARTESIAN_POINT('Ctrl Pts',(-24.7139589944422,26.5555661211502,8.31870287073323));
#45629=CARTESIAN_POINT('Ctrl Pts',(-24.7118860757095,26.5563679672524,8.3185645654007));
#45630=CARTESIAN_POINT('Ctrl Pts',(-24.7082457855265,26.5577717761143,8.3183220119863));
#45631=CARTESIAN_POINT('Ctrl Pts',(-24.7066787795218,26.5583746560185,8.31821770841885));
#45632=CARTESIAN_POINT('Ctrl Pts',(-24.7033561772978,26.5596499928583,8.31799677380087));
#45633=CARTESIAN_POINT('Ctrl Pts',(-24.7016004688582,26.5603221362711,8.31788016207136));
#45634=CARTESIAN_POINT('Ctrl Pts',(-24.6966029714595,26.5622303318655,8.31754861120656));
#45635=CARTESIAN_POINT('Ctrl Pts',(-24.6933597606162,26.5634626907987,8.31733389553557));
#45636=CARTESIAN_POINT('Ctrl Pts',(-24.6795874128415,26.5686704873514,8.31642398458779));
#45637=CARTESIAN_POINT('Ctrl Pts',(-24.6690393142162,26.5725960550055,8.31573175842992));
#45638=CARTESIAN_POINT('Ctrl Pts',(-24.4831411229539,26.6406731183705,8.30361035364273));
#45639=CARTESIAN_POINT('Ctrl Pts',(-24.3025333375933,26.6895321394603,8.29304662955898));
#45640=CARTESIAN_POINT('Ctrl Pts',(-23.971170453199,26.7489092952372,8.27418545002759));
#45641=CARTESIAN_POINT('Ctrl Pts',(-23.821992115627,26.7650205472064,8.26587520129653));
#45642=CARTESIAN_POINT('Ctrl Pts',(-23.6483952946672,26.7715961782197,8.25599952081196));
#45643=CARTESIAN_POINT('Ctrl Pts',(-23.6245427974422,26.7722345023612,8.25463837406028));
#45644=CARTESIAN_POINT('Ctrl Pts',(-23.5061900466449,26.77408684447,8.24785805053681));
#45645=CARTESIAN_POINT('Ctrl Pts',(-23.4116821212831,26.7714084006475,8.2423581229887));
#45646=CARTESIAN_POINT('Ctrl Pts',(-23.2671489964203,26.7609396526013,8.23373010488521));
#45647=CARTESIAN_POINT('Ctrl Pts',(-23.2169587996909,26.7561181329836,8.23069399606373));
#45648=CARTESIAN_POINT('Ctrl Pts',(-23.161210594475,26.7494394312346,8.22727079363634));
#45649=CARTESIAN_POINT('Ctrl Pts',(-23.1555186583866,26.7487421151853,8.22692069138754));
#45650=CARTESIAN_POINT('Ctrl Pts',(-23.1447813887312,26.7473976001791,8.22625913111292));
#45651=CARTESIAN_POINT('Ctrl Pts',(-23.1397356613743,26.7467536400041,8.22594777621598));
#45652=CARTESIAN_POINT('Ctrl Pts',(-23.1312192925016,26.7456462424979,8.22542145811859));
#45653=CARTESIAN_POINT('Ctrl Pts',(-23.1277478315432,26.7451890883082,8.22520669415515));
#45654=CARTESIAN_POINT('Ctrl Pts',(-23.1208792143201,26.7442731747058,8.22478131496989));
#45655=CARTESIAN_POINT('Ctrl Pts',(-23.1174820309084,26.7438146505758,8.2245707074665));
#45656=CARTESIAN_POINT('Ctrl Pts',(-23.109995320567,26.7427919900362,8.22410608938111));
#45657=CARTESIAN_POINT('Ctrl Pts',(-23.1059061373006,26.7422254148125,8.22385200175497));
#45658=CARTESIAN_POINT('Ctrl Pts',(-23.091624156121,26.7402186041142,8.22296345463544));
#45659=CARTESIAN_POINT('Ctrl Pts',(-23.0814372613615,26.7387374020406,8.22232769713919));
#45660=CARTESIAN_POINT('Ctrl Pts',(-22.9769909550334,26.7230392703957,8.21578858793561));
#45661=CARTESIAN_POINT('Ctrl Pts',(-22.8834083168583,26.7046970485344,8.20975445659271));
#45662=CARTESIAN_POINT('Ctrl Pts',(-22.6259677819104,26.6422707573087,8.19263880578794));
#45663=CARTESIAN_POINT('Ctrl Pts',(-22.464583432327,26.5893624159407,8.18130077763559));
#45664=CARTESIAN_POINT('Ctrl Pts',(-22.2289912941689,26.490956817984,8.16404267294249));
#45665=CARTESIAN_POINT('Ctrl Pts',(-22.1512327745749,26.4547673447831,8.15822689933198));
#45666=CARTESIAN_POINT('Ctrl Pts',(-22.075035838959,26.4155366837419,8.15244980096843));
#45667=CARTESIAN_POINT('Ctrl Pts',(-22.0750360380806,26.4155367862613,7.90859913775027));
#45668=CARTESIAN_POINT('Ctrl Pts',(-22.1212966157915,26.4393544466329,7.91209765527108));
#45669=CARTESIAN_POINT('Ctrl Pts',(-22.1681346141975,26.4620520920954,7.91557745044412));
#45670=CARTESIAN_POINT('Ctrl Pts',(-22.2760532281321,26.5111574932639,7.92342594061295));
#45671=CARTESIAN_POINT('Ctrl Pts',(-22.3374401273027,26.5368273991184,7.92777046036409));
#45672=CARTESIAN_POINT('Ctrl Pts',(-22.4262960460565,26.5707917714342,7.93384737801415));
#45673=CARTESIAN_POINT('Ctrl Pts',(-22.453146133568,26.580647418644,7.93565660817201));
#45674=CARTESIAN_POINT('Ctrl Pts',(-22.4843250998948,26.5916232916931,7.93772348727388));
#45675=CARTESIAN_POINT('Ctrl Pts',(-22.4885283088318,26.5930931559785,7.93800141074821));
#45676=CARTESIAN_POINT('Ctrl Pts',(-22.4949100508139,26.5953100211863,7.9384222904637));
#45677=CARTESIAN_POINT('Ctrl Pts',(-22.4970863385605,26.5960633984394,7.93856562553367));
#45678=CARTESIAN_POINT('Ctrl Pts',(-22.501026957483,26.5974228152571,7.93882481273498));
#45679=CARTESIAN_POINT('Ctrl Pts',(-22.5027910020285,26.5980296538823,7.93894071242398));
#45680=CARTESIAN_POINT('Ctrl Pts',(-22.506335780753,26.5992456313266,7.93917335266004));
#45681=CARTESIAN_POINT('Ctrl Pts',(-22.5081165144121,26.5998547395287,7.93929009115026));
#45682=CARTESIAN_POINT('Ctrl Pts',(-22.5131908053321,26.6015854607113,7.93962237803307));
#45683=CARTESIAN_POINT('Ctrl Pts',(-22.5164856596664,26.6027033048531,7.93983770137244));
#45684=CARTESIAN_POINT('Ctrl Pts',(-22.5305223122431,26.6074401813383,7.94075317724377));
#45685=CARTESIAN_POINT('Ctrl Pts',(-22.5412815234598,26.6110079219806,7.94145031559819));
#45686=CARTESIAN_POINT('Ctrl Pts',(-22.7291424839303,26.6722041353058,7.95354662072114));
#45687=CARTESIAN_POINT('Ctrl Pts',(-22.9109227927993,26.7144401359785,7.96408518876877));
#45688=CARTESIAN_POINT('Ctrl Pts',(-23.397850460784,26.7838654443096,7.99164390346882));
#45689=CARTESIAN_POINT('Ctrl Pts',(-23.7048915982453,26.7837557066122,8.00850615539715));
#45690=CARTESIAN_POINT('Ctrl Pts',(-24.0192728476122,26.7387135061588,8.02774124451109));
#45691=CARTESIAN_POINT('Ctrl Pts',(-24.0312189840206,26.7369333610203,8.02847484531774));
#45692=CARTESIAN_POINT('Ctrl Pts',(-24.0495393141961,26.7340980070445,8.02960411431868));
#45693=CARTESIAN_POINT('Ctrl Pts',(-24.0559208992355,26.7330906996195,8.02999826662405));
#45694=CARTESIAN_POINT('Ctrl Pts',(-24.0664219297063,26.7314007757498,8.03064816957189));
#45695=CARTESIAN_POINT('Ctrl Pts',(-24.0705431748086,26.730729326851,8.03090356550762));
#45696=CARTESIAN_POINT('Ctrl Pts',(-24.0785158505415,26.7294144772337,8.03139828886352));
#45697=CARTESIAN_POINT('Ctrl Pts',(-24.0823674414748,26.7287720821422,8.03163758393549));
#45698=CARTESIAN_POINT('Ctrl Pts',(-24.0893945102075,26.7275869282863,8.03207470958279));
#45699=CARTESIAN_POINT('Ctrl Pts',(-24.0925703642361,26.7270464043199,8.03227246875263));
#45700=CARTESIAN_POINT('Ctrl Pts',(-24.099086429782,26.7259273271625,8.03267863856926));
#45701=CARTESIAN_POINT('Ctrl Pts',(-24.1024265483862,26.7253482640167,8.03288706523334));
#45702=CARTESIAN_POINT('Ctrl Pts',(-24.1119646491451,26.7236791753748,8.0334828984526));
#45703=CARTESIAN_POINT('Ctrl Pts',(-24.1181603351732,26.7225762685724,8.03387071535205));
#45704=CARTESIAN_POINT('Ctrl Pts',(-24.1447383103226,26.7177647122339,8.03553773604119));
#45705=CARTESIAN_POINT('Ctrl Pts',(-24.165087449699,26.7138777854465,8.03682261905959));
#45706=CARTESIAN_POINT('Ctrl Pts',(-24.5235110400513,26.6418259365914,8.05960913765149));
#45707=CARTESIAN_POINT('Ctrl Pts',(-24.8484584709887,26.5200325523019,8.08306949723859));
#45708=CARTESIAN_POINT('Ctrl Pts',(-25.2791481093562,26.2742025068544,8.11645299052329));
#45709=CARTESIAN_POINT('Ctrl Pts',(-25.4050566696986,26.1900816702109,8.1264854446279));
#45710=CARTESIAN_POINT('Ctrl Pts',(-25.5291361676184,26.0939054118031,8.1363177889767));
#45711=CARTESIAN_POINT('Ctrl Pts',(-25.5336572801594,26.0903816669915,8.13667596256107));
#45712=CARTESIAN_POINT('Ctrl Pts',(-25.5401788454504,26.0852707463635,8.13719245712185));
#45713=CARTESIAN_POINT('Ctrl Pts',(-25.5421868180476,26.0836932517117,8.13735146244009));
#45714=CARTESIAN_POINT('Ctrl Pts',(-25.5456823625131,26.0809403724056,8.13762822258328));
#45715=CARTESIAN_POINT('Ctrl Pts',(-25.5471707737668,26.0797660603,8.13774605452433));
#45716=CARTESIAN_POINT('Ctrl Pts',(-25.5500546505338,26.0774866357169,8.13797433347576));
#45717=CARTESIAN_POINT('Ctrl Pts',(-25.5514502330247,26.0763816834358,8.13808479156712));
#45718=CARTESIAN_POINT('Ctrl Pts',(-25.5547863077491,26.0737358470659,8.1383488097111));
#45719=CARTESIAN_POINT('Ctrl Pts',(-25.556725943309,26.0721938773412,8.13850229146845));
#45720=CARTESIAN_POINT('Ctrl Pts',(-25.5636796459412,26.0666527288549,8.13905246215529));
#45721=CARTESIAN_POINT('Ctrl Pts',(-25.5686835940055,26.0626407869268,8.13944823911214));
#45722=CARTESIAN_POINT('Ctrl Pts',(-25.6437303150859,26.0021027529293,8.14538250364992));
#45723=CARTESIAN_POINT('Ctrl Pts',(-25.7113946234139,25.9426753803961,8.15071485179274));
#45724=CARTESIAN_POINT('Ctrl Pts',(-25.8470429967791,25.8130809760465,8.16158220323306));
#45725=CARTESIAN_POINT('Ctrl Pts',(-25.9145037108877,25.7425019359737,8.1670914573662));
#45726=CARTESIAN_POINT('Ctrl Pts',(-26.0899562155985,25.5414034256509,8.18205587057764));
#45727=CARTESIAN_POINT('Ctrl Pts',(-26.191023970195,25.4052730702022,8.19142440878584));
#45728=CARTESIAN_POINT('Ctrl Pts',(-26.3376356816523,25.1713672060007,8.20718562660294));
#45729=CARTESIAN_POINT('Ctrl Pts',(-26.3898055229627,25.0781442833416,8.21338574377907));
#45730=CARTESIAN_POINT('Ctrl Pts',(-26.4587947432071,24.9390829319715,8.2226384471591));
#45731=CARTESIAN_POINT('Ctrl Pts',(-26.479355800829,24.8951768150773,8.22555984294994));
#45732=CARTESIAN_POINT('Ctrl Pts',(-26.5020931114405,24.8436266683897,8.22899565790881));
#45733=CARTESIAN_POINT('Ctrl Pts',(-26.5052418694249,24.8364163929021,8.22947634902831));
#45734=CARTESIAN_POINT('Ctrl Pts',(-26.5099953860003,24.8254218124167,8.23020954857767));
#45735=CARTESIAN_POINT('Ctrl Pts',(-26.5116193756198,24.8216458121401,8.23046139911188));
#45736=CARTESIAN_POINT('Ctrl Pts',(-26.5144260280766,24.815085405027,8.23089903487267));
#45737=CARTESIAN_POINT('Ctrl Pts',(-26.5156120052801,24.8123024143983,8.23108470671077));
#45738=CARTESIAN_POINT('Ctrl Pts',(-26.5180711408746,24.8065092521113,8.23147125544782));
#45739=CARTESIAN_POINT('Ctrl Pts',(-26.5193436416291,24.8034988065232,8.23167215450587));
#45740=CARTESIAN_POINT('Ctrl Pts',(-26.522818333991,24.7952434842538,8.23222314225965));
#45741=CARTESIAN_POINT('Ctrl Pts',(-26.5250112142424,24.7899947229905,8.23257354731746));
#45742=CARTESIAN_POINT('Ctrl Pts',(-26.5333635743977,24.7698532053452,8.23391853345596));
#45743=CARTESIAN_POINT('Ctrl Pts',(-26.5394251243895,24.7549203249751,8.23491643093377));
#45744=CARTESIAN_POINT('Ctrl Pts',(-26.6365719424712,24.51034696466,8.25127378739768));
#45745=CARTESIAN_POINT('Ctrl Pts',(-26.7010479566851,24.271077003911,8.26756978276075));
#45746=CARTESIAN_POINT('Ctrl Pts',(-26.7612397577237,23.8685326980362,8.29505539645285));
#45747=CARTESIAN_POINT('Ctrl Pts',(-26.7730847377883,23.7086716858235,8.30596155425315));
#45748=CARTESIAN_POINT('Ctrl Pts',(-26.7729540622555,23.4555243342009,8.3227265290296));
#45749=CARTESIAN_POINT('Ctrl Pts',(-26.7688748168057,23.3624946551144,8.32877609515968));
#45750=CARTESIAN_POINT('Ctrl Pts',(-26.7602108055362,23.2633253687827,8.33501704747616));
#45751=CARTESIAN_POINT('Ctrl Pts',(-26.7596290471725,23.2568897865697,8.33542110954034));
#45752=CARTESIAN_POINT('Ctrl Pts',(-26.7587966907662,23.2479809305018,8.3359791092887));
#45753=CARTESIAN_POINT('Ctrl Pts',(-26.7585625864425,23.24550618749,8.33613396888424));
#45754=CARTESIAN_POINT('Ctrl Pts',(-26.7581557274082,23.2412576684563,8.33639957393928));
#45755=CARTESIAN_POINT('Ctrl Pts',(-26.7579843646992,23.2394837653393,8.33651039823266));
#45756=CARTESIAN_POINT('Ctrl Pts',(-26.7576461796473,23.2360130424883,8.33672708312222));
#45757=CARTESIAN_POINT('Ctrl Pts',(-26.757479482605,23.2343162171191,8.3368329503125));
#45758=CARTESIAN_POINT('Ctrl Pts',(-26.7570714723611,23.2301966425051,8.33708980901462));
#45759=CARTESIAN_POINT('Ctrl Pts',(-26.7568287594671,23.2277740269834,8.33724072078007));
#45760=CARTESIAN_POINT('Ctrl Pts',(-26.7560687811289,23.2202740715022,8.3377074870878));
#45761=CARTESIAN_POINT('Ctrl Pts',(-26.7555421968605,23.215197651776,8.33802281545169));
#45762=CARTESIAN_POINT('Ctrl Pts',(-26.7492600043566,23.156005993375,8.34169272290107));
#45763=CARTESIAN_POINT('Ctrl Pts',(-26.7421462091938,23.1020396755507,8.34497179279391));
#45764=CARTESIAN_POINT('Ctrl Pts',(-26.7234289304278,22.9833392392724,8.35208722548512));
#45765=CARTESIAN_POINT('Ctrl Pts',(-26.7112043225033,22.9187274426189,8.35589613942054));
#45766=CARTESIAN_POINT('Ctrl Pts',(-26.6235759694993,22.5223829931758,8.37910715031988));
#45767=CARTESIAN_POINT('Ctrl Pts',(-26.4980265589085,22.2039689530081,8.39734114433901));
#45768=CARTESIAN_POINT('Ctrl Pts',(-26.2979968701983,21.865368094769,8.42071761386771));
#45769=CARTESIAN_POINT('Ctrl Pts',(-26.2698779145882,21.8203473933895,8.42391019581193));
#45770=CARTESIAN_POINT('Ctrl Pts',(-26.2358499827951,21.7687474731935,8.42767691307078));
#45771=CARTESIAN_POINT('Ctrl Pts',(-26.2310089903571,21.7614711728383,8.42821061219945));
#45772=CARTESIAN_POINT('Ctrl Pts',(-26.2237478875708,21.7506529802548,8.42900793243711));
#45773=CARTESIAN_POINT('Ctrl Pts',(-26.221350177536,21.7470960411113,8.42927070613535));
#45774=CARTESIAN_POINT('Ctrl Pts',(-26.2170601085741,21.7407591718175,8.42973996471255));
#45775=CARTESIAN_POINT('Ctrl Pts',(-26.2151704830173,21.737977391402,8.42994634566487));
#45776=CARTESIAN_POINT('Ctrl Pts',(-26.211176526839,21.7321175098907,8.43038190532559));
#45777=CARTESIAN_POINT('Ctrl Pts',(-26.2090712026781,21.7290400948579,8.43061112163977));
#45778=CARTESIAN_POINT('Ctrl Pts',(-26.2034941193982,21.7209181883168,8.43121732921147));
#45779=CARTESIAN_POINT('Ctrl Pts',(-26.2000133271131,21.7158799444551,8.43159466476931));
#45780=CARTESIAN_POINT('Ctrl Pts',(-26.1841804382223,21.693101858592,8.43330648989124));
#45781=CARTESIAN_POINT('Ctrl Pts',(-26.1716646380853,21.6754769794784,8.4346472438909));
#45782=CARTESIAN_POINT('Ctrl Pts',(-26.0784938539611,21.5470301196691,8.44454003171268));
#45783=CARTESIAN_POINT('Ctrl Pts',(-25.9910301339395,21.441342860974,8.45336007573995));
#45784=CARTESIAN_POINT('Ctrl Pts',(-25.7904914470126,21.2282595232036,8.47266302867951));
#45785=CARTESIAN_POINT('Ctrl Pts',(-25.6758101730521,21.122842396553,8.48318726143137));
#45786=CARTESIAN_POINT('Ctrl Pts',(-25.4022050280378,20.9056468739201,8.50683113051343));
#45787=CARTESIAN_POINT('Ctrl Pts',(-25.2398577530878,20.7990854706112,8.51991124981041));
#45788=CARTESIAN_POINT('Ctrl Pts',(-25.0582822018522,20.7020760932013,8.53289124846135));
#45789=CARTESIAN_POINT('Ctrl Pts',(-25.0476313574047,20.6964622145755,8.53364685178423));
#45790=CARTESIAN_POINT('Ctrl Pts',(-25.033788490599,20.6892647108215,8.53462119685486));
#45791=CARTESIAN_POINT('Ctrl Pts',(-25.0306251358594,20.6876266033419,8.53484333365114));
#45792=CARTESIAN_POINT('Ctrl Pts',(-25.0257715123533,20.6851234062478,8.53518336127414));
#45793=CARTESIAN_POINT('Ctrl Pts',(-25.0240831974669,20.6842545665104,8.53530148992276));
#45794=CARTESIAN_POINT('Ctrl Pts',(-25.0207517340334,20.6825438527866,8.53553429237204));
#45795=CARTESIAN_POINT('Ctrl Pts',(-25.0191086385039,20.6817019031214,8.53564897039494));
#45796=CARTESIAN_POINT('Ctrl Pts',(-25.0154868842574,20.6798499833351,8.53590143583168));
#45797=CARTESIAN_POINT('Ctrl Pts',(-25.0135079094587,20.6788406495233,8.53603918238165));
#45798=CARTESIAN_POINT('Ctrl Pts',(-25.0078575332793,20.6759661542096,8.5364318996918));
#45799=CARTESIAN_POINT('Ctrl Pts',(-25.0041835813975,20.6741059736072,8.53668655527253));
#45800=CARTESIAN_POINT('Ctrl Pts',(-24.9959008938861,20.669932242565,8.53725911960972));
#45801=CARTESIAN_POINT('Ctrl Pts',(-24.9912901375239,20.6676226951524,8.53757677992103));
#45802=CARTESIAN_POINT('Ctrl Pts',(-24.8365450862406,20.5905743040348,8.54820280752068));
#45803=CARTESIAN_POINT('Ctrl Pts',(-24.6807853984301,20.5276449034363,8.55779448953633));
#45804=CARTESIAN_POINT('Ctrl Pts',(-24.265274285589,20.3964176513425,8.58231237733002));
#45805=CARTESIAN_POINT('Ctrl Pts',(-24.0006896542555,20.3479048898667,8.59698956182451));
#45806=CARTESIAN_POINT('Ctrl Pts',(-23.6607527554434,20.3285811978673,8.61704140567542));
#45807=CARTESIAN_POINT('Ctrl Pts',(-23.588237749468,20.326910732647,8.62137930249063));
#45808=CARTESIAN_POINT('Ctrl Pts',(-23.5061599636176,20.3277899570676,8.62637836573433));
#45809=CARTESIAN_POINT('Ctrl Pts',(-23.4965883816556,20.3279351427149,8.62696269641176));
#45810=CARTESIAN_POINT('Ctrl Pts',(-23.4826140401443,20.3282093916388,8.62781784007091));
#45811=CARTESIAN_POINT('Ctrl Pts',(-23.4782106103974,20.3283048407489,8.62808759734863));
#45812=CARTESIAN_POINT('Ctrl Pts',(-23.4704192602244,20.3284897072035,8.62856542719746));
#45813=CARTESIAN_POINT('Ctrl Pts',(-23.4670312523014,20.3285754425028,8.62877338383992));
#45814=CARTESIAN_POINT('Ctrl Pts',(-23.4600073482871,20.3287642731759,8.62920488015155));
#45815=CARTESIAN_POINT('Ctrl Pts',(-23.45637148044,20.3288681800618,8.62942844501741));
#45816=CARTESIAN_POINT('Ctrl Pts',(-23.4470234957408,20.3291511689531,8.63000376963261));
#45817=CARTESIAN_POINT('Ctrl Pts',(-23.4413116831125,20.3293392894981,8.63035581284039));
#45818=CARTESIAN_POINT('Ctrl Pts',(-23.4180849171385,20.3301661250665,8.63178946491573));
#45819=CARTESIAN_POINT('Ctrl Pts',(-23.4005750674499,20.3309325131727,8.63287507719618));
#45820=CARTESIAN_POINT('Ctrl Pts',(-23.2849027796125,20.3369410945609,8.64007962502133));
#45821=CARTESIAN_POINT('Ctrl Pts',(-23.1870273771757,20.3465289184664,8.64633458895748));
#45822=CARTESIAN_POINT('Ctrl Pts',(-22.9442757532686,20.3815755451505,8.66226263979204));
#45823=CARTESIAN_POINT('Ctrl Pts',(-22.8004224509638,20.4125035818414,8.67208178317791));
#45824=CARTESIAN_POINT('Ctrl Pts',(-22.4247137120696,20.5205970067321,8.69848196923771));
#45825=CARTESIAN_POINT('Ctrl Pts',(-22.1986323472732,20.6144741789378,8.71520291483597));
#45826=CARTESIAN_POINT('Ctrl Pts',(-21.9732195941979,20.7396875322024,8.73148739548046));
#45827=CARTESIAN_POINT('Ctrl Pts',(-21.9611830604198,20.7464753054924,8.73235550754247));
#45828=CARTESIAN_POINT('Ctrl Pts',(-21.9459696959232,20.7551840322618,8.73345054192751));
#45829=CARTESIAN_POINT('Ctrl Pts',(-21.9427522572708,20.7570332059469,8.73368200259418));
#45830=CARTESIAN_POINT('Ctrl Pts',(-21.9376632781504,20.7599697240406,8.73404789290686));
#45831=CARTESIAN_POINT('Ctrl Pts',(-21.9357896393625,20.761053396336,8.73418256014115));
#45832=CARTESIAN_POINT('Ctrl Pts',(-21.932303189376,20.7630745739325,8.73443306233311));
#45833=CARTESIAN_POINT('Ctrl Pts',(-21.9306901107767,20.7640115860252,8.73454892806822));
#45834=CARTESIAN_POINT('Ctrl Pts',(-21.9271278600629,20.7660849804494,8.73480472564117));
#45835=CARTESIAN_POINT('Ctrl Pts',(-21.9251790720987,20.7672220065192,8.73494461438896));
#45836=CARTESIAN_POINT('Ctrl Pts',(-21.9195385821656,20.7705209116245,8.73534936375295));
#45837=CARTESIAN_POINT('Ctrl Pts',(-21.915849970721,20.7726881068808,8.73561387819089));
#45838=CARTESIAN_POINT('Ctrl Pts',(-21.9075122120077,20.7776092075888,8.73621142320065));
#45839=CARTESIAN_POINT('Ctrl Pts',(-21.9028656393559,20.7803674819913,8.73654417314357));
#45840=CARTESIAN_POINT('Ctrl Pts',(-21.7851635559057,20.8506381287567,8.74496707679133));
#45841=CARTESIAN_POINT('Ctrl Pts',(-21.6763282589843,20.9250145735171,8.75261725830812));
#45842=CARTESIAN_POINT('Ctrl Pts',(-21.4161021337198,21.1273040292365,8.77135263853859));
#45843=CARTESIAN_POINT('Ctrl Pts',(-21.2713832610021,21.2628880171032,8.78221273123673));
#45844=CARTESIAN_POINT('Ctrl Pts',(-21.0239600428047,21.541639476319,8.80333313088229));
#45845=CARTESIAN_POINT('Ctrl Pts',(-20.9187560232081,21.6815918691193,8.81347876206296));
#45846=CARTESIAN_POINT('Ctrl Pts',(-20.8192870933154,21.8390899174721,8.82480664380453));
#45847=CARTESIAN_POINT('Ctrl Pts',(-20.8132006392869,21.8488423369251,8.82550763069144));
#45848=CARTESIAN_POINT('Ctrl Pts',(-20.8048345379281,21.8624085400167,8.82648220600942));
#45849=CARTESIAN_POINT('Ctrl Pts',(-20.8025103519581,21.8661948681583,8.82675415203712));
#45850=CARTESIAN_POINT('Ctrl Pts',(-20.798527471922,21.8727135679028,8.82722225106653));
#45851=CARTESIAN_POINT('Ctrl Pts',(-20.7968649952568,21.8754436310441,8.82741826478684));
#45852=CARTESIAN_POINT('Ctrl Pts',(-20.7934483524402,21.8810731633247,8.82782239894562));
#45853=CARTESIAN_POINT('Ctrl Pts',(-20.7916946933555,21.8839729336239,8.82803053761587));
#45854=CARTESIAN_POINT('Ctrl Pts',(-20.787633980049,21.8907115229573,8.82851414927054));
#45855=CARTESIAN_POINT('Ctrl Pts',(-20.7853303521335,21.8945523890889,8.82878974719933));
#45856=CARTESIAN_POINT('Ctrl Pts',(-20.7780573743829,21.906736218444,8.82966383295542));
#45857=CARTESIAN_POINT('Ctrl Pts',(-20.7731177580741,21.9150967874368,8.83026340426924));
#45858=CARTESIAN_POINT('Ctrl Pts',(-20.720347017574,22.0053430116168,8.83673316296633));
#45859=CARTESIAN_POINT('Ctrl Pts',(-20.6761192108494,22.0892716159403,8.84273293274057));
#45860=CARTESIAN_POINT('Ctrl Pts',(-20.6017547280566,22.2468758207101,8.85398636158182));
#45861=CARTESIAN_POINT('Ctrl Pts',(-20.5705215999902,22.3199549295507,8.85919905601402));
#45862=CARTESIAN_POINT('Ctrl Pts',(-20.4631811437182,22.5992496950615,8.87906949633699));
#45863=CARTESIAN_POINT('Ctrl Pts',(-20.4055360492379,22.8118997131531,8.89414297754651));
#45864=CARTESIAN_POINT('Ctrl Pts',(-20.3641774893267,23.0641170043646,8.91120121883877));
#45865=CARTESIAN_POINT('Ctrl Pts',(-20.3589683726862,23.0995780438729,8.91357979721791));
#45866=CARTESIAN_POINT('Ctrl Pts',(-20.3511411729773,23.1598357382444,8.91758088284595));
#45867=CARTESIAN_POINT('Ctrl Pts',(-20.3482174005271,23.1845889670626,8.91921288229018));
#45868=CARTESIAN_POINT('Ctrl Pts',(-20.3454023953977,23.2110534486138,8.92094368399854));
#45869=CARTESIAN_POINT('Ctrl Pts',(-20.3452251006871,23.212732783229,8.92105345381956));
#45870=CARTESIAN_POINT('Ctrl Pts',(-20.344802576429,23.2167652841061,8.92131689274395));
#45871=CARTESIAN_POINT('Ctrl Pts',(-20.3445586178114,23.2191185851347,8.9214705121963));
#45872=CARTESIAN_POINT('Ctrl Pts',(-20.3435525047375,23.2289291871993,8.92211042915794));
#45873=CARTESIAN_POINT('Ctrl Pts',(-20.3428137722328,23.2363889292139,8.92259579686318));
#45874=CARTESIAN_POINT('Ctrl Pts',(-20.3415001094199,23.2501435363502,8.92348843094332));
#45875=CARTESIAN_POINT('Ctrl Pts',(-20.340917659632,23.2564376294363,8.92389600906343));
#45876=CARTESIAN_POINT('Ctrl Pts',(-20.3369194552409,23.3010740801043,8.92677997508019));
#45877=CARTESIAN_POINT('Ctrl Pts',(-20.33417220573,23.3394753354339,8.92922713301581));
#45878=CARTESIAN_POINT('Ctrl Pts',(-20.3318598540093,23.3826558721342,8.93193391128876));
#45879=CARTESIAN_POINT('Ctrl Pts',(-20.3316166307622,23.3873936787359,8.93223029414352));
#45880=CARTESIAN_POINT('Ctrl Pts',(-20.3312659602958,23.39453229923,8.9326759322857));
#45881=CARTESIAN_POINT('Ctrl Pts',(-20.3311507367227,23.39693269819,8.93282562168555));
#45882=CARTESIAN_POINT('Ctrl Pts',(-20.3309557573381,23.4010917450178,8.93308470301539));
#45883=CARTESIAN_POINT('Ctrl Pts',(-20.3308747575987,23.4028503290115,8.93319416524176));
#45884=CARTESIAN_POINT('Ctrl Pts',(-20.3307089210712,23.4065161530836,8.93342216217588));
#45885=CARTESIAN_POINT('Ctrl Pts',(-20.3306243381385,23.4084234002739,8.93354068191174));
#45886=CARTESIAN_POINT('Ctrl Pts',(-20.3304295532102,23.412905555037,8.93381897341616));
#45887=CARTESIAN_POINT('Ctrl Pts',(-20.3303207448092,23.4154805290788,8.9339786662154));
#45888=CARTESIAN_POINT('Ctrl Pts',(-20.3299740024239,23.4239264424841,8.93450186251004));
#45889=CARTESIAN_POINT('Ctrl Pts',(-20.3297490336311,23.4297979462816,8.93486463823999));
#45890=CARTESIAN_POINT('Ctrl Pts',(-20.3292552953519,23.443676067056,8.9357199466054));
#45891=CARTESIAN_POINT('Ctrl Pts',(-20.3290003178443,23.451683179193,8.9362117239065));
#45892=CARTESIAN_POINT('Ctrl Pts',(-20.3282114851183,23.4797438127093,8.9379294396505));
#45893=CARTESIAN_POINT('Ctrl Pts',(-20.3278349996217,23.4998017646356,8.93914707761374));
#45894=CARTESIAN_POINT('Ctrl Pts',(-20.3269513763952,23.5935025225187,8.94479307487094));
#45895=CARTESIAN_POINT('Ctrl Pts',(-20.328781217753,23.6671505896015,8.94910922140287));
#45896=CARTESIAN_POINT('Ctrl Pts',(-20.3431630548736,23.9101244776603,8.96313349192628));
#45897=CARTESIAN_POINT('Ctrl Pts',(-20.3665650246052,24.0785245548232,8.9725183703753));
#45898=CARTESIAN_POINT('Ctrl Pts',(-20.4528670545767,24.4698542624448,8.99495730131921));
#45899=CARTESIAN_POINT('Ctrl Pts',(-20.5267008692826,24.6893645924753,9.00808771556767));
#45900=CARTESIAN_POINT('Ctrl Pts',(-20.62966139205,24.9127841752777,9.02301244191091));
#45901=CARTESIAN_POINT('Ctrl Pts',(-20.6360705147369,24.9264386545291,9.02393082670351));
#45902=CARTESIAN_POINT('Ctrl Pts',(-20.6449621336223,24.9450413695093,9.02519076542979));
#45903=CARTESIAN_POINT('Ctrl Pts',(-20.6473619439125,24.9500290974311,9.02552944187062));
#45904=CARTESIAN_POINT('Ctrl Pts',(-20.6511859265764,24.957924675826,9.02606694694528));
#45905=CARTESIAN_POINT('Ctrl Pts',(-20.6526016600799,24.9608366207804,9.02626548090226));
#45906=CARTESIAN_POINT('Ctrl Pts',(-20.6553524068347,24.9664728654275,9.0266503356672));
#45907=CARTESIAN_POINT('Ctrl Pts',(-20.6566868839321,24.9691974244169,9.02683663758455));
#45908=CARTESIAN_POINT('Ctrl Pts',(-20.6598688605097,24.9756708081405,9.02727990780957));
#45909=CARTESIAN_POINT('Ctrl Pts',(-20.6617198056478,24.979417924423,9.02753699657255));
#45910=CARTESIAN_POINT('Ctrl Pts',(-20.667223064191,24.9905045443085,9.02829914137707));
#45911=CARTESIAN_POINT('Ctrl Pts',(-20.6708960794395,24.9978336828562,9.02880492336293));
#45912=CARTESIAN_POINT('Ctrl Pts',(-20.6960228492536,25.047497664181,9.03224554843079));
#45913=CARTESIAN_POINT('Ctrl Pts',(-20.7183805930161,25.0893662381444,9.03521216815063));
#45914=CARTESIAN_POINT('Ctrl Pts',(-20.7714507153635,25.1836752280068,9.04205152337455));
#45915=CARTESIAN_POINT('Ctrl Pts',(-20.8027374357924,25.2357700344135,9.04594390233056));
#45916=CARTESIAN_POINT('Ctrl Pts',(-20.9074073886994,25.3993886460025,9.05854229728576));
#45917=CARTESIAN_POINT('Ctrl Pts',(-20.9862477809929,25.5072420912258,9.06742710590673));
#45918=CARTESIAN_POINT('Ctrl Pts',(-21.1592741939436,25.7154744482687,9.08566943292162));
#45919=CARTESIAN_POINT('Ctrl Pts',(-21.2536650885101,25.8153462457989,9.09501476061617));
#45920=CARTESIAN_POINT('Ctrl Pts',(-21.4297181053238,25.9792680245846,9.11114700274104));
#45921=CARTESIAN_POINT('Ctrl Pts',(-21.5086460282935,26.0459747613417,9.11798293101955));
#45922=CARTESIAN_POINT('Ctrl Pts',(-21.5947116745465,26.1118933566586,9.12492645203125));
#45923=CARTESIAN_POINT('Ctrl Pts',(-21.5987825567572,26.1149959297272,9.12525372475191));
#45924=CARTESIAN_POINT('Ctrl Pts',(-21.6068881186365,26.1211430131538,9.12590304209541));
#45925=CARTESIAN_POINT('Ctrl Pts',(-21.6109226050256,26.1241877573518,9.12622510016796));
#45926=CARTESIAN_POINT('Ctrl Pts',(-21.622236967678,26.1326847709488,9.1271250732373));
#45927=CARTESIAN_POINT('Ctrl Pts',(-21.6295328542827,26.1381157836098,9.12770169975395));
#45928=CARTESIAN_POINT('Ctrl Pts',(-21.6483735634865,26.1520171205858,9.12918104452008));
#45929=CARTESIAN_POINT('Ctrl Pts',(-21.6599521811021,26.1604416414096,9.13008085183502));
#45930=CARTESIAN_POINT('Ctrl Pts',(-21.6746424553593,26.1709811607204,9.13121034954066));
#45931=CARTESIAN_POINT('Ctrl Pts',(-21.677701947236,26.173168087795,9.13144492684119));
#45932=CARTESIAN_POINT('Ctrl Pts',(-21.6825377587891,26.1766119558075,9.13181464950696));
#45933=CARTESIAN_POINT('Ctrl Pts',(-21.6843115231953,26.1778724529207,9.13195004081434));
#45934=CARTESIAN_POINT('Ctrl Pts',(-21.6876076399254,26.1802097645628,9.1322012189221));
#45935=CARTESIAN_POINT('Ctrl Pts',(-21.689129640812,26.1812870477386,9.13231703793973));
#45936=CARTESIAN_POINT('Ctrl Pts',(-21.6921150151896,26.1833962304841,9.13254389405364));
#45937=CARTESIAN_POINT('Ctrl Pts',(-21.6935783069382,26.1844282266476,9.13265493782859));
#45938=CARTESIAN_POINT('Ctrl Pts',(-21.6980164630672,26.1875527301812,9.13299127944001));
#45939=CARTESIAN_POINT('Ctrl Pts',(-21.7009940234705,26.1896414308401,9.13321631414353));
#45940=CARTESIAN_POINT('Ctrl Pts',(-21.7158933737338,26.200055445365,9.13433931497765));
#45941=CARTESIAN_POINT('Ctrl Pts',(-21.7278681252211,26.2083052203341,9.13523215373943));
#45942=CARTESIAN_POINT('Ctrl Pts',(-21.7611327274915,26.2308917566385,9.13768681693809));
#45943=CARTESIAN_POINT('Ctrl Pts',(-21.7825391144246,26.2450559929775,9.13923778613895));
#45944=CARTESIAN_POINT('Ctrl Pts',(-21.8573049716843,26.2932529430453,9.14456475083909));
#45945=CARTESIAN_POINT('Ctrl Pts',(-21.9114987972983,26.3259704455679,9.14826928343459));
#45946=CARTESIAN_POINT('Ctrl Pts',(-22.0023926632846,26.3772534202516,9.15428783567698));
#45947=CARTESIAN_POINT('Ctrl Pts',(-22.0385366392128,26.396744753782,9.15663222934342));
#45948=CARTESIAN_POINT('Ctrl Pts',(-22.0750360476606,26.4155367911937,9.15896072794325));
#45949=CARTESIAN_POINT('Origin',(-23.5502525316942,23.5502525316942,-77.3107734492734));
#45950=CARTESIAN_POINT('',(-22.0750358939633,26.4155367120613,10.654266819213));
#45951=CARTESIAN_POINT('',(-22.0750360597002,26.4155367973924,10.4044010236784));
#45952=CARTESIAN_POINT('',(-22.0750360153461,26.4155367745563,-77.3107734492734));
#45953=CARTESIAN_POINT('Ctrl Pts',(-22.0750358939633,26.4155367120613,10.654266819213));
#45954=CARTESIAN_POINT('Ctrl Pts',(-22.0114257619618,26.3827864788733,10.6502545497521));
#45955=CARTESIAN_POINT('Ctrl Pts',(-21.9489028433,26.3479162601968,10.6462204514863));
#45956=CARTESIAN_POINT('Ctrl Pts',(-21.7940114567944,26.254631177202,10.6359072392353));
#45957=CARTESIAN_POINT('Ctrl Pts',(-21.7033824925041,26.1935675377572,10.6295707120918));
#45958=CARTESIAN_POINT('Ctrl Pts',(-21.5902202490526,26.1086568165435,10.6211405043412));
#45959=CARTESIAN_POINT('Ctrl Pts',(-21.5647001786132,26.0889019312882,10.6192033802087));
#45960=CARTESIAN_POINT('Ctrl Pts',(-21.523722684736,26.0561856903716,10.6160313122216));
#45961=CARTESIAN_POINT('Ctrl Pts',(-21.5080823489127,26.0434563204302,10.6148056110686));
#45962=CARTESIAN_POINT('Ctrl Pts',(-21.489154345466,26.0277535795707,10.6133034700161));
#45963=CARTESIAN_POINT('Ctrl Pts',(-21.4857517589214,26.0249189202029,10.6130326893305));
#45964=CARTESIAN_POINT('Ctrl Pts',(-21.4791743948838,26.0194163801552,10.6125077990431));
#45965=CARTESIAN_POINT('Ctrl Pts',(-21.4759989010499,26.0167493662398,10.612253725194));
#45966=CARTESIAN_POINT('Ctrl Pts',(-21.4705125267413,26.0121234161849,10.6118136054193));
#45967=CARTESIAN_POINT('Ctrl Pts',(-21.4681992390471,26.0101673323693,10.6116276769055));
#45968=CARTESIAN_POINT('Ctrl Pts',(-21.4634088909582,26.006105082929,10.6112419172777));
#45969=CARTESIAN_POINT('Ctrl Pts',(-21.4609322537915,26.003998425323,10.6110420659906));
#45970=CARTESIAN_POINT('Ctrl Pts',(-21.4549243359952,25.9988723269709,10.6105562563182));
#45971=CARTESIAN_POINT('Ctrl Pts',(-21.4513963959832,25.9958489969248,10.6102701372146));
#45972=CARTESIAN_POINT('Ctrl Pts',(-21.4381941979904,25.9844855334559,10.6091962446419));
#45973=CARTESIAN_POINT('Ctrl Pts',(-21.4285631125958,25.9760956249652,10.6084064053043));
#45974=CARTESIAN_POINT('Ctrl Pts',(-21.2720213498002,25.8380823371557,10.5954620358419));
#45975=CARTESIAN_POINT('Ctrl Pts',(-21.1372096571707,25.6954101369374,10.582734209057));
#45976=CARTESIAN_POINT('Ctrl Pts',(-20.9375838045897,25.4413556448599,10.5611284261831));
#45977=CARTESIAN_POINT('Ctrl Pts',(-20.8649630958745,25.3367371920506,10.5524922414885));
#45978=CARTESIAN_POINT('Ctrl Pts',(-20.7425704366555,25.1360237728624,10.5365987895456));
#45979=CARTESIAN_POINT('Ctrl Pts',(-20.6910749559801,25.0411769222699,10.5293431070927));
#45980=CARTESIAN_POINT('Ctrl Pts',(-20.6219162681521,24.8969799213987,10.5188410400439));
#45981=CARTESIAN_POINT('Ctrl Pts',(-20.6005418495196,24.8494967375762,10.5154642906458));
#45982=CARTESIAN_POINT('Ctrl Pts',(-20.5707495865267,24.7787834168032,10.5105757266236));
#45983=CARTESIAN_POINT('Ctrl Pts',(-20.5614339986934,24.755943123412,10.5090178694784));
#45984=CARTESIAN_POINT('Ctrl Pts',(-20.5507650317147,24.7289007801116,10.5072001162085));
#45985=CARTESIAN_POINT('Ctrl Pts',(-20.5491572269697,24.724800925138,10.5069252481421));
#45986=CARTESIAN_POINT('Ctrl Pts',(-20.5467183196721,24.7185440804105,10.5065068782936));
#45987=CARTESIAN_POINT('Ctrl Pts',(-20.5458811338398,24.7163894916712,10.5063630100716));
#45988=CARTESIAN_POINT('Ctrl Pts',(-20.5444368746334,24.712660654956,10.5061143735594));
#45989=CARTESIAN_POINT('Ctrl Pts',(-20.5438287204809,24.7110868336834,10.5060095396303));
#45990=CARTESIAN_POINT('Ctrl Pts',(-20.5425633519946,24.7078045657263,10.5057911286985));
#45991=CARTESIAN_POINT('Ctrl Pts',(-20.5419063590794,24.7060960413995,10.5056775653676));
#45992=CARTESIAN_POINT('Ctrl Pts',(-20.5400962701562,24.7013768678209,10.5053642348629));
#45993=CARTESIAN_POINT('Ctrl Pts',(-20.5389462314829,24.6983650360352,10.5051646529751));
#45994=CARTESIAN_POINT('Ctrl Pts',(-20.5344698902678,24.6865889686323,10.5043858022915));
#45995=CARTESIAN_POINT('Ctrl Pts',(-20.5311772714137,24.6778118499348,10.5038085443272));
#45996=CARTESIAN_POINT('Ctrl Pts',(-20.4727357912453,24.5199333252625,10.4934811947188));
#45997=CARTESIAN_POINT('Ctrl Pts',(-20.4286469599481,24.3669434021449,10.4843658988429));
#45998=CARTESIAN_POINT('Ctrl Pts',(-20.3562213934687,24.0213626631628,10.4644697182507));
#45999=CARTESIAN_POINT('Ctrl Pts',(-20.333652696768,23.8282186381666,10.4537889030883));
#46000=CARTESIAN_POINT('Ctrl Pts',(-20.3268080151372,23.5655940228441,10.4387890688568));
#46001=CARTESIAN_POINT('Ctrl Pts',(-20.3272126179922,23.4969344207244,10.4348267912876));
#46002=CARTESIAN_POINT('Ctrl Pts',(-20.3329812388142,23.3445468624452,10.4258897661041));
#46003=CARTESIAN_POINT('Ctrl Pts',(-20.3394223980521,23.2609130363562,10.4208883753321));
#46004=CARTESIAN_POINT('Ctrl Pts',(-20.3502098835418,23.1682394387018,10.4152060518849));
#46005=CARTESIAN_POINT('Ctrl Pts',(-20.3513443664597,23.1588531185484,10.4146289309233));
#46006=CARTESIAN_POINT('Ctrl Pts',(-20.3530771800223,23.1450274116994,10.4137764576133));
#46007=CARTESIAN_POINT('Ctrl Pts',(-20.353643496555,23.1405840030539,10.4135021184168));
#46008=CARTESIAN_POINT('Ctrl Pts',(-20.3546545144712,23.1327811452749,10.4130197179599));
#46009=CARTESIAN_POINT('Ctrl Pts',(-20.3550952552011,23.1294211824709,10.4128117823883));
#46010=CARTESIAN_POINT('Ctrl Pts',(-20.3559619597076,23.1228937614821,10.4124074127174));
#46011=CARTESIAN_POINT('Ctrl Pts',(-20.3563873375099,23.1197262281837,10.4122109974007));
#46012=CARTESIAN_POINT('Ctrl Pts',(-20.3574151312657,23.1121582221753,10.4117412603311));
#46013=CARTESIAN_POINT('Ctrl Pts',(-20.3580219326808,23.1077583599547,10.4114677998048));
#46014=CARTESIAN_POINT('Ctrl Pts',(-20.3602310104389,23.0919815878221,10.4104859171206));
#46015=CARTESIAN_POINT('Ctrl Pts',(-20.3618850126717,23.0806121137342,10.4097758562915));
#46016=CARTESIAN_POINT('Ctrl Pts',(-20.3895962383634,22.8970239055613,10.3982695513132));
#46017=CARTESIAN_POINT('Ctrl Pts',(-20.4295073432051,22.7272172173318,10.38702438803));
#46018=CARTESIAN_POINT('Ctrl Pts',(-20.5412161608102,22.3806766398056,10.3628257654625));
#46019=CARTESIAN_POINT('Ctrl Pts',(-20.6153739913148,22.2053776362976,10.3498535004855));
#46020=CARTESIAN_POINT('Ctrl Pts',(-20.7365298597034,21.97744274913,10.3325035214382));
#46021=CARTESIAN_POINT('Ctrl Pts',(-20.7704337078204,21.9182678161164,10.3279549295725));
#46022=CARTESIAN_POINT('Ctrl Pts',(-20.8336434631589,21.8156363734818,10.3200375580268));
#46023=CARTESIAN_POINT('Ctrl Pts',(-20.8621799214616,21.7717350648642,10.3166413105595));
#46024=CARTESIAN_POINT('Ctrl Pts',(-20.9058419357566,21.7080176253605,10.3117195270083));
#46025=CARTESIAN_POINT('Ctrl Pts',(-20.9201466564327,21.6876521914295,10.3101476002546));
#46026=CARTESIAN_POINT('Ctrl Pts',(-20.9372645344425,21.6638721980407,10.3083154756052));
#46027=CARTESIAN_POINT('Ctrl Pts',(-20.9398500684273,21.6602959138588,10.3080400320711));
#46028=CARTESIAN_POINT('Ctrl Pts',(-20.9438022321421,21.6548529034997,10.3076209668129));
#46029=CARTESIAN_POINT('Ctrl Pts',(-20.9451635263834,21.6529823376826,10.3074769767847));
#46030=CARTESIAN_POINT('Ctrl Pts',(-20.9475212474141,21.6497498950566,10.3072282039678));
#46031=CARTESIAN_POINT('Ctrl Pts',(-20.9485167279467,21.648387337317,10.3071233553186));
#46032=CARTESIAN_POINT('Ctrl Pts',(-20.950593751073,21.6455491075006,10.3069049866252));
#46033=CARTESIAN_POINT('Ctrl Pts',(-20.9516754771229,21.6440735785812,10.3067914801412));
#46034=CARTESIAN_POINT('Ctrl Pts',(-20.9546640801672,21.6400042450146,10.3064784907316));
#46035=CARTESIAN_POINT('Ctrl Pts',(-20.9565735948042,21.6374123661259,10.3062791924051));
#46036=CARTESIAN_POINT('Ctrl Pts',(-20.9640392731625,21.6273105633977,10.3055026223818));
#46037=CARTESIAN_POINT('Ctrl Pts',(-20.9696242672262,21.6198218549372,10.3049273466287));
#46038=CARTESIAN_POINT('Ctrl Pts',(-20.9806359710058,21.6051898683726,10.3038039150716));
#46039=CARTESIAN_POINT('Ctrl Pts',(-20.9860600902259,21.598044765948,10.303255595879));
#46040=CARTESIAN_POINT('Ctrl Pts',(-20.9958737552024,21.585228854682,10.3022724061693));
#46041=CARTESIAN_POINT('Ctrl Pts',(-21.0002525002768,21.579549909055,10.3018368489219));
#46042=CARTESIAN_POINT('Ctrl Pts',(-21.0068949163627,21.5709943370716,10.3011807508338));
#46043=CARTESIAN_POINT('Ctrl Pts',(-21.0091445597129,21.5681069176129,10.3009593394347));
#46044=CARTESIAN_POINT('Ctrl Pts',(-21.0150167204617,21.5605964209167,10.3003834449727));
#46045=CARTESIAN_POINT('Ctrl Pts',(-21.0186469832641,21.5559793794029,10.3000294374425));
#46046=CARTESIAN_POINT('Ctrl Pts',(-21.0862149276822,21.4705269178776,10.2934772930075));
#46047=CARTESIAN_POINT('Ctrl Pts',(-21.1539878458718,21.3927865160274,10.2875131148611));
#46048=CARTESIAN_POINT('Ctrl Pts',(-21.4006912620173,21.1357980347168,10.2672566247874));
#46049=CARTESIAN_POINT('Ctrl Pts',(-21.5969093008709,20.9744691217061,10.2534829997442));
#46050=CARTESIAN_POINT('Ctrl Pts',(-21.9035343671022,20.7777465943858,10.2324731251937));
#46051=CARTESIAN_POINT('Ctrl Pts',(-22.0001110944063,20.7226161775626,10.2259314646765));
#46052=CARTESIAN_POINT('Ctrl Pts',(-22.1162429256501,20.6640625582583,10.2180580565959));
#46053=CARTESIAN_POINT('Ctrl Pts',(-22.1332253066132,20.6556869455438,10.2169066355041));
#46054=CARTESIAN_POINT('Ctrl Pts',(-22.1555765708045,20.6449072677921,10.2153907782825));
#46055=CARTESIAN_POINT('Ctrl Pts',(-22.1608798611912,20.6423674376616,10.2150310798906));
#46056=CARTESIAN_POINT('Ctrl Pts',(-22.1695079920747,20.6382642801293,10.2144458116799));
#46057=CARTESIAN_POINT('Ctrl Pts',(-22.1728286237614,20.6366920915078,10.2142205501462));
#46058=CARTESIAN_POINT('Ctrl Pts',(-22.1792061605115,20.6336859180934,10.2137878864309));
#46059=CARTESIAN_POINT('Ctrl Pts',(-22.1822626466146,20.632251051625,10.2135805151857));
#46060=CARTESIAN_POINT('Ctrl Pts',(-22.1892377034797,20.6289899809911,10.2131072495706));
#46061=CARTESIAN_POINT('Ctrl Pts',(-22.1931576992186,20.6271668558822,10.212841249019));
#46062=CARTESIAN_POINT('Ctrl Pts',(-22.2034922323319,20.6223857049983,10.2121399044396));
#46063=CARTESIAN_POINT('Ctrl Pts',(-22.2099128208876,20.6194408835042,10.2117041050797));
#46064=CARTESIAN_POINT('Ctrl Pts',(-22.2421092348739,20.6048018316161,10.2095183568531));
#46065=CARTESIAN_POINT('Ctrl Pts',(-22.2680280021833,20.5934267192576,10.2077574657655));
#46066=CARTESIAN_POINT('Ctrl Pts',(-22.3004193763429,20.5797169157814,10.2055545629359));
#46067=CARTESIAN_POINT('Ctrl Pts',(-22.3067546731726,20.5770593263517,10.2051236000609));
#46068=CARTESIAN_POINT('Ctrl Pts',(-22.3223284931955,20.5705847586318,10.2040639066434));
#46069=CARTESIAN_POINT('Ctrl Pts',(-22.3315763245823,20.5667904855561,10.2034344182222));
#46070=CARTESIAN_POINT('Ctrl Pts',(-22.3424212431676,20.5623997834269,10.2026959256665));
#46071=CARTESIAN_POINT('Ctrl Pts',(-22.344001415514,20.5617614891163,10.2025883154505));
#46072=CARTESIAN_POINT('Ctrl Pts',(-22.3520531968881,20.5585164816259,10.202039949513));
#46073=CARTESIAN_POINT('Ctrl Pts',(-22.3585327135207,20.5559295509595,10.2015985401792));
#46074=CARTESIAN_POINT('Ctrl Pts',(-22.369381088894,20.551639154394,10.2008592968982));
#46075=CARTESIAN_POINT('Ctrl Pts',(-22.3737453790911,20.5499241379266,10.200561843267));
#46076=CARTESIAN_POINT('Ctrl Pts',(-22.3818541167625,20.5467580947328,10.2000090749873));
#46077=CARTESIAN_POINT('Ctrl Pts',(-22.3855975682215,20.5453045280342,10.1997538436161));
#46078=CARTESIAN_POINT('Ctrl Pts',(-22.3934838613298,20.5422592633436,10.1992160600866));
#46079=CARTESIAN_POINT('Ctrl Pts',(-22.3976272908432,20.5406691198213,10.1989334583733));
#46080=CARTESIAN_POINT('Ctrl Pts',(-22.4194085767439,20.5323615910385,10.1974475934335));
#46081=CARTESIAN_POINT('Ctrl Pts',(-22.4371016226992,20.5257907927492,10.1962396616554));
#46082=CARTESIAN_POINT('Ctrl Pts',(-22.6876737035053,20.4352305177069,10.1791189968194));
#46083=CARTESIAN_POINT('Ctrl Pts',(-22.9293859952176,20.3782040254862,10.1623413343034));
#46084=CARTESIAN_POINT('Ctrl Pts',(-23.3477256878194,20.329184764327,10.1338716710516));
#46085=CARTESIAN_POINT('Ctrl Pts',(-23.5216374532977,20.3229484006228,10.1222281043836));
#46086=CARTESIAN_POINT('Ctrl Pts',(-23.7057518442876,20.3312389254891,10.1106262390037));
#46087=CARTESIAN_POINT('Ctrl Pts',(-23.7162779684177,20.3317646577276,10.1099655106216));
#46088=CARTESIAN_POINT('Ctrl Pts',(-23.7300364661536,20.3325195104608,10.1091054121356));
#46089=CARTESIAN_POINT('Ctrl Pts',(-23.7332711827749,20.3327018743458,10.1089034521207));
#46090=CARTESIAN_POINT('Ctrl Pts',(-23.7385541177961,20.3330077033492,10.1085740339224));
#46091=CARTESIAN_POINT('Ctrl Pts',(-23.7406024929208,20.3331282466908,10.108446410986));
#46092=CARTESIAN_POINT('Ctrl Pts',(-23.7445334602574,20.3333633448335,10.1082016951737));
#46093=CARTESIAN_POINT('Ctrl Pts',(-23.74641606143,20.3334775956192,10.108084585721));
#46094=CARTESIAN_POINT('Ctrl Pts',(-23.7507429565837,20.333743997628,10.1078156283359));
#46095=CARTESIAN_POINT('Ctrl Pts',(-23.7531871840994,20.3338972827919,10.1076638448003));
#46096=CARTESIAN_POINT('Ctrl Pts',(-23.7609361739919,20.3343921145731,10.1071831054818));
#46097=CARTESIAN_POINT('Ctrl Pts',(-23.7662403024047,20.3347440021768,10.1068547315709));
#46098=CARTESIAN_POINT('Ctrl Pts',(-23.8111664751135,20.33783616893,10.1040790441649));
#46099=CARTESIAN_POINT('Ctrl Pts',(-23.8507377936744,20.3412957022526,10.1016714458111));
#46100=CARTESIAN_POINT('Ctrl Pts',(-23.8975977524443,20.3462669438034,10.0988539573671));
#46101=CARTESIAN_POINT('Ctrl Pts',(-23.9049556469169,20.3470731655292,10.0984125431298));
#46102=CARTESIAN_POINT('Ctrl Pts',(-23.9222045231954,20.3490233277439,10.0973799233608));
#46103=CARTESIAN_POINT('Ctrl Pts',(-23.9320931583028,20.350187776004,10.0967896087591));
#46104=CARTESIAN_POINT('Ctrl Pts',(-23.9462925932158,20.3519266037289,10.0959441649481));
#46105=CARTESIAN_POINT('Ctrl Pts',(-23.950607782581,20.352463898078,10.0956875291792));
#46106=CARTESIAN_POINT('Ctrl Pts',(-23.9636768159073,20.3541180225896,10.0949111329689));
#46107=CARTESIAN_POINT('Ctrl Pts',(-23.9724272322403,20.3552620834845,10.0943924553257));
#46108=CARTESIAN_POINT('Ctrl Pts',(-24.2645182163729,20.3946720490982,10.0771144231299));
#46109=CARTESIAN_POINT('Ctrl Pts',(-24.5415387855318,20.4704392189449,10.0617399871382));
#46110=CARTESIAN_POINT('Ctrl Pts',(-24.9053432699292,20.624209768643,10.0392098355348));
#46111=CARTESIAN_POINT('Ctrl Pts',(-25.0035114582854,20.6717056306109,10.0328859065209));
#46112=CARTESIAN_POINT('Ctrl Pts',(-25.1420110045653,20.7476074887997,10.0234747490309));
#46113=CARTESIAN_POINT('Ctrl Pts',(-25.1843992732781,20.7721095727227,10.0205250264729));
#46114=CARTESIAN_POINT('Ctrl Pts',(-25.232928210657,20.8016561694468,10.0170604589054));
#46115=CARTESIAN_POINT('Ctrl Pts',(-25.2396300431923,20.8057702444406,10.0165800338997));
#46116=CARTESIAN_POINT('Ctrl Pts',(-25.2498396087567,20.8120891883154,10.0158451156775));
#46117=CARTESIAN_POINT('Ctrl Pts',(-25.2533582920892,20.8142763811775,10.0155912754888));
#46118=CARTESIAN_POINT('Ctrl Pts',(-25.2596869733633,20.8182271916611,10.0151337175826));
#46119=CARTESIAN_POINT('Ctrl Pts',(-25.2624984887638,20.8199883775664,10.0149300901455));
#46120=CARTESIAN_POINT('Ctrl Pts',(-25.2685326437524,20.8237812715702,10.0144922880063));
#46121=CARTESIAN_POINT('Ctrl Pts',(-25.2717544076802,20.8258143572158,10.0142580623582));
#46122=CARTESIAN_POINT('Ctrl Pts',(-25.2804517642747,20.8313243882109,10.0136244689582));
#46123=CARTESIAN_POINT('Ctrl Pts',(-25.2859204560128,20.8348121457983,10.0132246990771));
#46124=CARTESIAN_POINT('Ctrl Pts',(-25.3102268868345,20.8504174390503,10.011441662621));
#46125=CARTESIAN_POINT('Ctrl Pts',(-25.3289481597964,20.8627144240605,10.0100516972492));
#46126=CARTESIAN_POINT('Ctrl Pts',(-25.6287686291538,21.0641551222702,9.98751693373543));
#46127=CARTESIAN_POINT('Ctrl Pts',(-25.8783873431475,21.2962386195797,9.96449421718862));
#46128=CARTESIAN_POINT('Ctrl Pts',(-26.1829230411643,21.6849785310592,9.93122724731233));
#46129=CARTESIAN_POINT('Ctrl Pts',(-26.2696916598121,21.8139157066536,9.92091675488752));
#46130=CARTESIAN_POINT('Ctrl Pts',(-26.3496913552182,21.9536020425832,9.91083481968869));
#46131=CARTESIAN_POINT('Ctrl Pts',(-26.3525307550793,21.958590736279,9.91047614260217));
#46132=CARTESIAN_POINT('Ctrl Pts',(-26.3566146895984,21.9658108228871,9.90995906050701));
#46133=CARTESIAN_POINT('Ctrl Pts',(-26.3578699024113,21.9680361148658,9.90979996896176));
#46134=CARTESIAN_POINT('Ctrl Pts',(-26.3600520174968,21.9719154298777,9.90952311366748));
#46135=CARTESIAN_POINT('Ctrl Pts',(-26.3609801074187,21.9735687801054,9.90940527262999));
#46136=CARTESIAN_POINT('Ctrl Pts',(-26.3627764302843,21.9767754746579,9.90917701736984));
#46137=CARTESIAN_POINT('Ctrl Pts',(-26.3636448334625,21.9783287149812,9.90906659200037));
#46138=CARTESIAN_POINT('Ctrl Pts',(-26.3657185015278,21.9820449350017,9.90880271492932));
#46139=CARTESIAN_POINT('Ctrl Pts',(-26.3669225631973,21.9842085899916,9.90864934134456));
#46140=CARTESIAN_POINT('Ctrl Pts',(-26.3712315014598,21.9919726405366,9.90809990281217));
#46141=CARTESIAN_POINT('Ctrl Pts',(-26.3743222052459,21.9975809477329,9.90770474670204));
#46142=CARTESIAN_POINT('Ctrl Pts',(-26.4203057292261,22.0816129369644,9.90180915660264));
#46143=CARTESIAN_POINT('Ctrl Pts',(-26.4599389953425,22.1617872908641,9.89651202471771));
#46144=CARTESIAN_POINT('Ctrl Pts',(-26.6172348139953,22.5163982764757,9.87403292326879));
#46145=CARTESIAN_POINT('Ctrl Pts',(-26.6997830209683,22.8047857037683,9.85801234086306));
#46146=CARTESIAN_POINT('Ctrl Pts',(-26.7529737118501,23.1821444172696,9.83601893386724));
#46147=CARTESIAN_POINT('Ctrl Pts',(-26.7613478469282,23.2642598824024,9.83118364245458));
#46148=CARTESIAN_POINT('Ctrl Pts',(-26.7692477265032,23.389024671387,9.82370999942974));
#46149=CARTESIAN_POINT('Ctrl Pts',(-26.771094172069,23.4314949987661,9.8211439883325));
#46150=CARTESIAN_POINT('Ctrl Pts',(-26.7722797778683,23.4815816879287,9.81808809973317));
#46151=CARTESIAN_POINT('Ctrl Pts',(-26.7724326811429,23.4891759992756,9.81762395390833));
#46152=CARTESIAN_POINT('Ctrl Pts',(-26.7726259866295,23.5008227546305,9.81691087981366));
#46153=CARTESIAN_POINT('Ctrl Pts',(-26.7726855961948,23.5048748884383,9.81666255489299));
#46154=CARTESIAN_POINT('Ctrl Pts',(-26.7727804280571,23.5122697131915,9.81620895321523));
#46155=CARTESIAN_POINT('Ctrl Pts',(-26.7728180929389,23.5156123717067,9.81600375344587));
#46156=CARTESIAN_POINT('Ctrl Pts',(-26.7728883382005,23.5228452988839,9.81555938903561));
#46157=CARTESIAN_POINT('Ctrl Pts',(-26.7729190751632,23.526735576521,9.81532016682901));
#46158=CARTESIAN_POINT('Ctrl Pts',(-26.7729833958779,23.5372970219284,9.81467012266586));
#46159=CARTESIAN_POINT('Ctrl Pts',(-26.7730033093116,23.543968226646,9.81425887212319));
#46160=CARTESIAN_POINT('Ctrl Pts',(-26.772999057819,23.5793841912314,9.81207215828765));
#46161=CARTESIAN_POINT('Ctrl Pts',(-26.7726110314294,23.6081268620325,9.8102853094006));
#46162=CARTESIAN_POINT('Ctrl Pts',(-26.7636347353523,23.9420240309938,9.78938006149644));
#46163=CARTESIAN_POINT('Ctrl Pts',(-26.7121133467723,24.2444138632098,9.76878854226643));
#46164=CARTESIAN_POINT('Ctrl Pts',(-26.5724002238423,24.67980205695,9.73787743807381));
#46165=CARTESIAN_POINT('Ctrl Pts',(-26.5157169699548,24.8211928189896,9.72766593036809));
#46166=CARTESIAN_POINT('Ctrl Pts',(-26.4473820904776,24.9619097768698,9.71765261287181));
#46167=CARTESIAN_POINT('Ctrl Pts',(-26.4455059250084,24.9657537316819,9.71737920548148));
#46168=CARTESIAN_POINT('Ctrl Pts',(-26.4414195537452,24.9740839206039,9.71678699842042));
#46169=CARTESIAN_POINT('Ctrl Pts',(-26.4392065418069,24.9785687787576,9.71646834582569));
#46170=CARTESIAN_POINT('Ctrl Pts',(-26.4328808213499,24.9913135455803,9.71556338090899));
#46171=CARTESIAN_POINT('Ctrl Pts',(-26.4287430269699,24.9995610479356,9.71497842362775));
#46172=CARTESIAN_POINT('Ctrl Pts',(-26.4181478909131,25.0204550332429,9.7134984320716));
#46173=CARTESIAN_POINT('Ctrl Pts',(-26.4116421991446,25.033076990542,9.712606172948));
#46174=CARTESIAN_POINT('Ctrl Pts',(-26.4033136245163,25.0489766614569,9.7114848811479));
#46175=CARTESIAN_POINT('Ctrl Pts',(-26.4015682912596,25.0522944938585,9.71125104567565));
#46176=CARTESIAN_POINT('Ctrl Pts',(-26.3988020566558,25.0575308368223,9.71088223961336));
#46177=CARTESIAN_POINT('Ctrl Pts',(-26.3977850042356,25.0594513599331,9.71074702507237));
#46178=CARTESIAN_POINT('Ctrl Pts',(-26.3958916423835,25.0630179105632,9.7104960201257));
#46179=CARTESIAN_POINT('Ctrl Pts',(-26.3950158523741,25.0646641960494,9.71038019784211));
#46180=CARTESIAN_POINT('Ctrl Pts',(-26.3930607440312,25.0683316733856,9.71012226394974));
#46181=CARTESIAN_POINT('Ctrl Pts',(-26.3919807013475,25.0703524700029,9.70998019972637));
#46182=CARTESIAN_POINT('Ctrl Pts',(-26.3888215657474,25.0762481866551,9.70956589023506));
#46183=CARTESIAN_POINT('Ctrl Pts',(-26.3867366852842,25.0801200249835,9.70929401407809));
#46184=CARTESIAN_POINT('Ctrl Pts',(-26.3716782458132,25.1079485013646,9.70734134985502));
#46185=CARTESIAN_POINT('Ctrl Pts',(-26.3584087865055,25.1317449792265,9.70567918642833));
#46186=CARTESIAN_POINT('Ctrl Pts',(-26.316712698874,25.2043398000426,9.70062301898617));
#46187=CARTESIAN_POINT('Ctrl Pts',(-26.2873027030324,25.2525638215775,9.69728465467246));
#46188=CARTESIAN_POINT('Ctrl Pts',(-26.2122338981055,25.368675428995,9.6892346597337));
#46189=CARTESIAN_POINT('Ctrl Pts',(-26.1652281688687,25.4356465209913,9.68458071872071));
#46190=CARTESIAN_POINT('Ctrl Pts',(-25.914883504586,25.7649207650677,9.66126896494603));
#46191=CARTESIAN_POINT('Ctrl Pts',(-25.6744804934729,25.9964494213852,9.64318862987));
#46192=CARTESIAN_POINT('Ctrl Pts',(-25.38558494636,26.1994267563148,9.6218472952312));
#46193=CARTESIAN_POINT('Ctrl Pts',(-25.3680770605265,26.2114708792732,9.62055640143095));
#46194=CARTESIAN_POINT('Ctrl Pts',(-25.3451800488028,26.2268909392013,9.61887083718964));
#46195=CARTESIAN_POINT('Ctrl Pts',(-25.3398979747377,26.2304255006451,9.61848218098158));
#46196=CARTESIAN_POINT('Ctrl Pts',(-25.331457406695,26.2360375282145,9.61786140065487));
#46197=CARTESIAN_POINT('Ctrl Pts',(-25.3283056340829,26.2381251140822,9.61762965823046));
#46198=CARTESIAN_POINT('Ctrl Pts',(-25.3226311205042,26.2418692965731,9.61721253224171));
#46199=CARTESIAN_POINT('Ctrl Pts',(-25.3201097080586,26.2435279068128,9.61702722465354));
#46200=CARTESIAN_POINT('Ctrl Pts',(-25.3142032316264,26.2474013698149,9.61659322371564));
#46201=CARTESIAN_POINT('Ctrl Pts',(-25.3108163253293,26.2496133921706,9.61634442460059));
#46202=CARTESIAN_POINT('Ctrl Pts',(-25.3010864423463,26.2559419742088,9.61562986164836));
#46203=CARTESIAN_POINT('Ctrl Pts',(-25.2947331618613,26.260042573641,9.61516350215529));
#46204=CARTESIAN_POINT('Ctrl Pts',(-25.2538125784584,26.2862504043605,9.61216111373683));
#46205=CARTESIAN_POINT('Ctrl Pts',(-25.2188414917677,26.3077172773216,9.60960142432445));
#46206=CARTESIAN_POINT('Ctrl Pts',(-25.1135637650723,26.369605556149,9.60190955620714));
#46207=CARTESIAN_POINT('Ctrl Pts',(-25.0421354715868,26.4080448479951,9.5967079626743));
#46208=CARTESIAN_POINT('Ctrl Pts',(-24.7227494426512,26.5646845734089,9.57352002744865));
#46209=CARTESIAN_POINT('Ctrl Pts',(-24.4617236595673,26.6535948366625,9.55462346320315));
#46210=CARTESIAN_POINT('Ctrl Pts',(-24.1559165144712,26.7158005101852,9.53378972004817));
#46211=CARTESIAN_POINT('Ctrl Pts',(-24.1190527170591,26.7226316682266,9.53130149402064));
#46212=CARTESIAN_POINT('Ctrl Pts',(-24.0042287886528,26.7418435345227,9.52363828318648));
#46213=CARTESIAN_POINT('Ctrl Pts',(-23.9259202170361,26.7520057764936,9.51853574023417));
#46214=CARTESIAN_POINT('Ctrl Pts',(-23.841112123262,26.7598564022402,9.51319755999968));
#46215=CARTESIAN_POINT('Ctrl Pts',(-23.8349123370484,26.7604122013341,9.51280840040594));
#46216=CARTESIAN_POINT('Ctrl Pts',(-23.8262741035326,26.7611613807758,9.51226772227356));
#46217=CARTESIAN_POINT('Ctrl Pts',(-23.8238370391775,26.7613699482009,9.51211535421511));
#46218=CARTESIAN_POINT('Ctrl Pts',(-23.8196344810058,26.7617247900526,9.51185290293051));
#46219=CARTESIAN_POINT('Ctrl Pts',(-23.8178691044347,26.7618723832411,9.51174274501014));
#46220=CARTESIAN_POINT('Ctrl Pts',(-23.8142090889729,26.7621753377624,9.51151455216016));
#46221=CARTESIAN_POINT('Ctrl Pts',(-23.812314437244,26.7623304781249,9.51139653042299));
#46222=CARTESIAN_POINT('Ctrl Pts',(-23.8078956102732,26.762688370603,9.51112151564151));
#46223=CARTESIAN_POINT('Ctrl Pts',(-23.8053713244894,26.762889824747,9.51096459634618));
#46224=CARTESIAN_POINT('Ctrl Pts',(-23.7972069141976,26.7635317135134,9.5104576553628));
#46225=CARTESIAN_POINT('Ctrl Pts',(-23.7915658263767,26.7639602754556,9.51010830199799));
#46226=CARTESIAN_POINT('Ctrl Pts',(-23.7783149303232,26.7649318792744,9.50928974904194));
#46227=CARTESIAN_POINT('Ctrl Pts',(-23.7707042259364,26.7654627610039,9.5088212177828));
#46228=CARTESIAN_POINT('Ctrl Pts',(-23.6893193113883,26.7708494000177,9.5038274898316));
#46229=CARTESIAN_POINT('Ctrl Pts',(-23.615394105057,26.7731925380821,9.49943629577195));
#46230=CARTESIAN_POINT('Ctrl Pts',(-23.4108415405854,26.772633665587,9.48752610757906));
#46231=CARTESIAN_POINT('Ctrl Pts',(-23.2803685149324,26.7643376284446,9.48019701891813));
#46232=CARTESIAN_POINT('Ctrl Pts',(-23.0477836495362,26.7352816342032,9.46708939423936));
#46233=CARTESIAN_POINT('Ctrl Pts',(-22.9454983155951,26.7174527512905,9.46131017670366));
#46234=CARTESIAN_POINT('Ctrl Pts',(-22.6587915114503,26.6530810303466,9.44472931339738));
#46235=CARTESIAN_POINT('Ctrl Pts',(-22.4774063646374,26.5951223488322,9.43375869578466));
#46236=CARTESIAN_POINT('Ctrl Pts',(-22.2905968592045,26.5166549856943,9.42144609262112));
#46237=CARTESIAN_POINT('Ctrl Pts',(-22.2790231085889,26.5117136033821,9.42067909180608));
#46238=CARTESIAN_POINT('Ctrl Pts',(-22.2632430637916,26.5048668060765,9.41962751612401));
#46239=CARTESIAN_POINT('Ctrl Pts',(-22.259011375932,26.5030199045429,9.41934494356333));
#46240=CARTESIAN_POINT('Ctrl Pts',(-22.2518138150707,26.499860129613,9.41886333887613));
#46241=CARTESIAN_POINT('Ctrl Pts',(-22.2488459192774,26.4985518569952,9.41866446468593));
#46242=CARTESIAN_POINT('Ctrl Pts',(-22.2431076115636,26.4960120113952,9.41827939407669));
#46243=CARTESIAN_POINT('Ctrl Pts',(-22.2403369520721,26.49478100475,9.41809321730081));
#46244=CARTESIAN_POINT('Ctrl Pts',(-22.2337638973252,26.4918494769087,9.41765093720547));
#46245=CARTESIAN_POINT('Ctrl Pts',(-22.2299630606637,26.4901454931716,9.41739471496134));
#46246=CARTESIAN_POINT('Ctrl Pts',(-22.2187524443579,26.4850934463618,9.41663757146618));
#46247=CARTESIAN_POINT('Ctrl Pts',(-22.211352061066,26.4817247223849,9.41613593852285));
#46248=CARTESIAN_POINT('Ctrl Pts',(-22.1605252907426,26.458355287734,9.41267797581846));
#46249=CARTESIAN_POINT('Ctrl Pts',(-22.1175386100646,26.4374196051673,9.40968941864562));
#46250=CARTESIAN_POINT('Ctrl Pts',(-22.0750360149249,26.4155367743394,9.40666775021339));
#46251=CARTESIAN_POINT('',(-26.7730012638346,23.5531112005712,9.56507739177766));
#46252=CARTESIAN_POINT('Ctrl Pts',(-22.0750360476606,26.4155367911937,9.15896072794325));
#46253=CARTESIAN_POINT('Ctrl Pts',(-22.1583267955234,26.4584197560539,9.16427430419078));
#46254=CARTESIAN_POINT('Ctrl Pts',(-22.2434683747133,26.4976611756449,9.1695061070461));
#46255=CARTESIAN_POINT('Ctrl Pts',(-22.57608362442,26.6337040788026,9.18958538803959));
#46256=CARTESIAN_POINT('Ctrl Pts',(-22.8333933469615,26.7034675760865,9.2044842187267));
#46257=CARTESIAN_POINT('Ctrl Pts',(-23.1129501123843,26.7432395341934,9.22159733060522));
#46258=CARTESIAN_POINT('Ctrl Pts',(-23.1295888604008,26.7454741927175,9.22261880629557));
#46259=CARTESIAN_POINT('Ctrl Pts',(-23.1519838047304,26.7483039781564,9.22399783954222));
#46260=CARTESIAN_POINT('Ctrl Pts',(-23.1577254552396,26.7490137804679,9.22435176654865));
#46261=CARTESIAN_POINT('Ctrl Pts',(-23.1667329274327,26.7501026976941,9.22490759319267));
#46262=CARTESIAN_POINT('Ctrl Pts',(-23.1699974906551,26.7504922844842,9.22510916151078));
#46263=CARTESIAN_POINT('Ctrl Pts',(-23.1762626754245,26.7512302378049,9.22549623556743));
#46264=CARTESIAN_POINT('Ctrl Pts',(-23.1792632034328,26.7515793825214,9.22568171650463));
#46265=CARTESIAN_POINT('Ctrl Pts',(-23.1863085179171,26.7523891449319,9.22611747435042));
#46266=CARTESIAN_POINT('Ctrl Pts',(-23.1903536882655,26.7528463175589,9.22636785981343));
#46267=CARTESIAN_POINT('Ctrl Pts',(-23.2020340293893,26.7541439842134,9.22709139299253));
#46268=CARTESIAN_POINT('Ctrl Pts',(-23.2096713138245,26.7549648428495,9.22756515993356));
#46269=CARTESIAN_POINT('Ctrl Pts',(-23.2605051331313,26.7602447174578,9.2307231579031));
#46270=CARTESIAN_POINT('Ctrl Pts',(-23.303783312234,26.7638573633208,9.23343395980405));
#46271=CARTESIAN_POINT('Ctrl Pts',(-23.4523087600109,26.7732377112293,9.24281871401772));
#46272=CARTESIAN_POINT('Ctrl Pts',(-23.55774979958,26.7747162467735,9.24962397153464));
#46273=CARTESIAN_POINT('Ctrl Pts',(-23.6889733090509,26.7701199471366,9.25826571057158));
#46274=CARTESIAN_POINT('Ctrl Pts',(-23.7148692590524,26.7688999047676,9.25997929072323));
#46275=CARTESIAN_POINT('Ctrl Pts',(-23.90126398205,26.7578629343217,9.2723693790412));
#46276=CARTESIAN_POINT('Ctrl Pts',(-24.0608367894398,26.7363585528252,9.28329211165587));
#46277=CARTESIAN_POINT('Ctrl Pts',(-24.3627835287042,26.6723953187608,9.30414990529683));
#46278=CARTESIAN_POINT('Ctrl Pts',(-24.5051758802602,26.6318288746371,9.31406585226229));
#46279=CARTESIAN_POINT('Ctrl Pts',(-24.6486747983109,26.5800392911524,9.3238353675773));
#46280=CARTESIAN_POINT('Ctrl Pts',(-24.6530552117312,26.5784476266389,9.32413336148684));
#46281=CARTESIAN_POINT('Ctrl Pts',(-24.6623287805766,26.5750551970638,9.32476372439559));
#46282=CARTESIAN_POINT('Ctrl Pts',(-24.66722105931,26.5732520449089,9.32509597367348));
#46283=CARTESIAN_POINT('Ctrl Pts',(-24.680070230751,26.5684807620328,9.32596777243583));
#46284=CARTESIAN_POINT('Ctrl Pts',(-24.6880198674389,26.5654930157655,9.32650630925608));
#46285=CARTESIAN_POINT('Ctrl Pts',(-24.6989570556881,26.5613330315561,9.327245990374));
#46286=CARTESIAN_POINT('Ctrl Pts',(-24.7019547213058,26.5601877347735,9.32744859323432));
#46287=CARTESIAN_POINT('Ctrl Pts',(-24.7163079456354,26.5546793188199,9.32841804731137));
#46288=CARTESIAN_POINT('Ctrl Pts',(-24.7276406526046,26.550256326952,9.3291815805187));
#46289=CARTESIAN_POINT('Ctrl Pts',(-24.7422727423089,26.5444499487968,9.330164680193));
#46290=CARTESIAN_POINT('Ctrl Pts',(-24.7455950489978,26.5431251687639,9.33038771647948));
#46291=CARTESIAN_POINT('Ctrl Pts',(-24.7506803798343,26.5410875589344,9.33072882225837));
#46292=CARTESIAN_POINT('Ctrl Pts',(-24.7524449760967,26.5403787005075,9.33084713195368));
#46293=CARTESIAN_POINT('Ctrl Pts',(-24.7559213653692,26.5389786205154,9.33108010490143));
#46294=CARTESIAN_POINT('Ctrl Pts',(-24.7576331830736,26.538287493539,9.33119477269725));
#46295=CARTESIAN_POINT('Ctrl Pts',(-24.7609983131798,26.536925496477,9.33142008934035));
#46296=CARTESIAN_POINT('Ctrl Pts',(-24.7626516547375,26.5362547273449,9.33153074365644));
#46297=CARTESIAN_POINT('Ctrl Pts',(-24.7663583404249,26.534747319867,9.33177871923271));
#46298=CARTESIAN_POINT('Ctrl Pts',(-24.7684113824629,26.5339099337806,9.33191599496229));
#46299=CARTESIAN_POINT('Ctrl Pts',(-24.7777522452705,26.5300887739676,9.33254024753811));
#46300=CARTESIAN_POINT('Ctrl Pts',(-24.7850300614542,26.5270803790291,9.33302573889215));
#46301=CARTESIAN_POINT('Ctrl Pts',(-24.8029615585778,26.519591049354,9.3342199010479));
#46302=CARTESIAN_POINT('Ctrl Pts',(-24.8136023957874,26.51507938475,9.33492677101193));
#46303=CARTESIAN_POINT('Ctrl Pts',(-24.8545740916084,26.4974469473966,9.33764254872906));
#46304=CARTESIAN_POINT('Ctrl Pts',(-24.8847278604639,26.4839166981611,9.3396285984888));
#46305=CARTESIAN_POINT('Ctrl Pts',(-24.9964736060865,26.431695835367,9.34696035299412));
#46306=CARTESIAN_POINT('Ctrl Pts',(-25.0766415908517,26.3900429972723,9.35216382884057));
#46307=CARTESIAN_POINT('Ctrl Pts',(-25.2187517019879,26.3084474212308,9.36146854096072));
#46308=CARTESIAN_POINT('Ctrl Pts',(-25.2812724451053,26.2696456868055,9.36559234386658));
#46309=CARTESIAN_POINT('Ctrl Pts',(-25.4288687659926,26.1708898120042,9.37552378619351));
#46310=CARTESIAN_POINT('Ctrl Pts',(-25.5124732861423,26.1088904428256,9.3813168945732));
#46311=CARTESIAN_POINT('Ctrl Pts',(-25.7401940315848,25.9222817598008,9.39792859240034));
#46312=CARTESIAN_POINT('Ctrl Pts',(-25.8764503586455,25.7888131638589,9.40891602758545));
#46313=CARTESIAN_POINT('Ctrl Pts',(-26.0083110400416,25.6345329333341,9.4212486538743));
#46314=CARTESIAN_POINT('Ctrl Pts',(-26.0164436429954,25.6249037839733,9.42201683573491));
#46315=CARTESIAN_POINT('Ctrl Pts',(-26.0274799458272,25.6116800101105,9.42306979212775));
#46316=CARTESIAN_POINT('Ctrl Pts',(-26.0304327854314,25.6081263904894,9.42335255760914));
#46317=CARTESIAN_POINT('Ctrl Pts',(-26.0354461010337,25.6020666099687,9.42383441530304));
#46318=CARTESIAN_POINT('Ctrl Pts',(-26.0375104593923,25.5995636573848,9.42403334924495));
#46319=CARTESIAN_POINT('Ctrl Pts',(-26.041496530981,25.5947158084627,9.42441847498305));
#46320=CARTESIAN_POINT('Ctrl Pts',(-26.0434187222781,25.5923713088639,9.42460464703693));
#46321=CARTESIAN_POINT('Ctrl Pts',(-26.0479729248483,25.5868005268418,9.42504682160047));
#46322=CARTESIAN_POINT('Ctrl Pts',(-26.050601992821,25.5835718550916,9.42530294284314));
#46323=CARTESIAN_POINT('Ctrl Pts',(-26.0583413639303,25.5740296804317,9.42605945786255));
#46324=CARTESIAN_POINT('Ctrl Pts',(-26.0634340354701,25.5677019772274,9.42656056150282));
#46325=CARTESIAN_POINT('Ctrl Pts',(-26.0997930884796,25.5221741205263,9.43016207894104));
#46326=CARTESIAN_POINT('Ctrl Pts',(-26.1301632802207,25.4822700975826,9.43329808889174));
#46327=CARTESIAN_POINT('Ctrl Pts',(-26.254705628078,25.310456140014,9.44672522327764));
#46328=CARTESIAN_POINT('Ctrl Pts',(-26.3397749346718,25.172268107692,9.45735779162834));
#46329=CARTESIAN_POINT('Ctrl Pts',(-26.4394053947308,24.9792247632555,9.47191472380165));
#46330=CARTESIAN_POINT('Ctrl Pts',(-26.463461411714,24.9295203382765,9.47563630302654));
#46331=CARTESIAN_POINT('Ctrl Pts',(-26.4974362825707,24.8544627212158,9.4812049326555));
#46332=CARTESIAN_POINT('Ctrl Pts',(-26.5083305596401,24.8295611928029,9.48304414395847));
#46333=CARTESIAN_POINT('Ctrl Pts',(-26.5307461980921,24.7765070723564,9.48694268576868));
#46334=CARTESIAN_POINT('Ctrl Pts',(-26.5421866702694,24.748322984817,9.4890019646958));
#46335=CARTESIAN_POINT('Ctrl Pts',(-26.59855619592,24.6036088894269,9.49950600975966));
#46336=CARTESIAN_POINT('Ctrl Pts',(-26.6370863484994,24.484691521539,9.50791366539804));
#46337=CARTESIAN_POINT('Ctrl Pts',(-26.6695689435786,24.3601888560918,9.51631432739777));
#46338=CARTESIAN_POINT('Ctrl Pts',(-26.6705126771592,24.3565455007143,9.5165598057875));
#46339=CARTESIAN_POINT('Ctrl Pts',(-26.6724175917225,24.3491380008965,9.51705817405828));
#46340=CARTESIAN_POINT('Ctrl Pts',(-26.6733783534086,24.3453737532531,9.51731104746704));
#46341=CARTESIAN_POINT('Ctrl Pts',(-26.6761267323784,24.3345238152638,9.51803880690306));
#46342=CARTESIAN_POINT('Ctrl Pts',(-26.6778970703135,24.3274337246252,9.51851300693196));
#46343=CARTESIAN_POINT('Ctrl Pts',(-26.6800240843095,24.3187901888501,9.51908939132572));
#46344=CARTESIAN_POINT('Ctrl Pts',(-26.6804037292492,24.3172424810962,9.51919253163381));
#46345=CARTESIAN_POINT('Ctrl Pts',(-26.6824302249699,24.3089544522432,9.51974449158068));
#46346=CARTESIAN_POINT('Ctrl Pts',(-26.6840564663185,24.3022090513894,9.52019244234582));
#46347=CARTESIAN_POINT('Ctrl Pts',(-26.6949285582426,24.256465385041,9.52322133855341));
#46348=CARTESIAN_POINT('Ctrl Pts',(-26.7034685326044,24.2173006010444,9.52577103316768));
#46349=CARTESIAN_POINT('Ctrl Pts',(-26.7123142449377,24.1727569010233,9.52861392726454));
#46350=CARTESIAN_POINT('Ctrl Pts',(-26.7133394109521,24.1675266713047,9.52894684792257));
#46351=CARTESIAN_POINT('Ctrl Pts',(-26.7148172212889,24.1598867653613,9.5294318347485));
#46352=CARTESIAN_POINT('Ctrl Pts',(-26.7152800912984,24.1574791125772,9.52958448347532));
#46353=CARTESIAN_POINT('Ctrl Pts',(-26.7160942688041,24.1532178849128,9.52985431110272));
#46354=CARTESIAN_POINT('Ctrl Pts',(-26.7164466964422,24.1513645285788,9.52997155456625));
#46355=CARTESIAN_POINT('Ctrl Pts',(-26.7171788421087,24.1474957926748,9.53021605219894));
#46356=CARTESIAN_POINT('Ctrl Pts',(-26.7175582630661,24.145480364089,9.53034328894474));
#46357=CARTESIAN_POINT('Ctrl Pts',(-26.7183240207792,24.141391307028,9.53060116545819));
#46358=CARTESIAN_POINT('Ctrl Pts',(-26.7187102461443,24.139317658365,9.53073179876874));
#46359=CARTESIAN_POINT('Ctrl Pts',(-26.7196565662239,24.1342089969917,9.531053283364));
#46360=CARTESIAN_POINT('Ctrl Pts',(-26.7202143390603,24.1311735482563,9.53124400236555));
#46361=CARTESIAN_POINT('Ctrl Pts',(-26.7217446684244,24.1227775272685,9.531770712314));
#46362=CARTESIAN_POINT('Ctrl Pts',(-26.722707999196,24.1174152522839,9.53210618510366));
#46363=CARTESIAN_POINT('Ctrl Pts',(-26.7563202363051,23.9275511883541,9.543952662313));
#46364=CARTESIAN_POINT('Ctrl Pts',(-26.7728350193474,23.7405285732528,9.55457143638722));
#46365=CARTESIAN_POINT('Ctrl Pts',(-26.7730012638346,23.5531112005712,9.56507739177766));
#46366=CARTESIAN_POINT('Ctrl Pts',(-26.7730012617393,23.5531135616897,9.5650772594217));
#46367=CARTESIAN_POINT('Ctrl Pts',(-26.7732594660026,23.2622646496,9.5813812232073));
#46368=CARTESIAN_POINT('Ctrl Pts',(-26.7341483716483,22.9727404047934,9.59741081275145));
#46369=CARTESIAN_POINT('Ctrl Pts',(-26.6508830654244,22.6712248915581,9.61619688286547));
#46370=CARTESIAN_POINT('Ctrl Pts',(-26.6448246833606,22.6501289509257,9.61752178419563));
#46371=CARTESIAN_POINT('Ctrl Pts',(-26.6356848506449,22.6194864243494,9.61946225669596));
#46372=CARTESIAN_POINT('Ctrl Pts',(-26.6327734793119,22.6098894393948,9.62007229715068));
#46373=CARTESIAN_POINT('Ctrl Pts',(-26.6274589248023,22.592660553741,9.62117167590116));
#46374=CARTESIAN_POINT('Ctrl Pts',(-26.6250720158306,22.5850236882684,9.6216604785591));
#46375=CARTESIAN_POINT('Ctrl Pts',(-26.6214074382732,22.5734504899288,9.62240352323699));
#46376=CARTESIAN_POINT('Ctrl Pts',(-26.6201505738228,22.5695075599087,9.6226570798158));
#46377=CARTESIAN_POINT('Ctrl Pts',(-26.6178631321862,22.5623790700897,9.62311622640468));
#46378=CARTESIAN_POINT('Ctrl Pts',(-26.6168351772588,22.5591926696378,9.62332172966447));
#46379=CARTESIAN_POINT('Ctrl Pts',(-26.6147739508377,22.5528373001323,9.62373214732872));
#46380=CARTESIAN_POINT('Ctrl Pts',(-26.6137407247162,22.5496683205337,9.62393706002642));
#46381=CARTESIAN_POINT('Ctrl Pts',(-26.6108302863364,22.5407885614183,9.62451199276973));
#46382=CARTESIAN_POINT('Ctrl Pts',(-26.6089420163196,22.5350814449536,9.62488237811046));
#46383=CARTESIAN_POINT('Ctrl Pts',(-26.601191332594,22.5118736814275,9.6263921052055));
#46384=CARTESIAN_POINT('Ctrl Pts',(-26.5951946906331,22.4944185346002,9.62753588708407));
#46385=CARTESIAN_POINT('Ctrl Pts',(-26.4878053690423,22.1903529559902,9.64760819452844));
#46386=CARTESIAN_POINT('Ctrl Pts',(-26.3465300324249,21.9195203719462,9.6680115792069));
#46387=CARTESIAN_POINT('Ctrl Pts',(-26.1274408433168,21.61390938295,9.69345473667857));
#46388=CARTESIAN_POINT('Ctrl Pts',(-26.0834397793119,21.5566910754048,9.69832756584687));
#46389=CARTESIAN_POINT('Ctrl Pts',(-25.9645341693013,21.412368380956,9.71083040500302));
#46390=CARTESIAN_POINT('Ctrl Pts',(-25.8868201136967,21.3276948303605,9.71837987664804));
#46391=CARTESIAN_POINT('Ctrl Pts',(-25.7965119205114,21.2392854226906,9.72634292847421));
#46392=CARTESIAN_POINT('Ctrl Pts',(-25.7882383030415,21.2312721700771,9.72706543536277));
#46393=CARTESIAN_POINT('Ctrl Pts',(-25.7781238406935,21.2215805510566,9.72793998751222));
#46394=CARTESIAN_POINT('Ctrl Pts',(-25.7763239228131,21.2198598770948,9.72809528536088));
#46395=CARTESIAN_POINT('Ctrl Pts',(-25.7731666630712,21.2168486157447,9.7283671096234));
#46396=CARTESIAN_POINT('Ctrl Pts',(-25.7718101901205,21.2155571252709,9.7284837062347));
#46397=CARTESIAN_POINT('Ctrl Pts',(-25.7690761900943,21.2129586389162,9.72871832758051));
#46398=CARTESIAN_POINT('Ctrl Pts',(-25.7676986305437,21.2116516749712,9.72883634978317));
#46399=CARTESIAN_POINT('Ctrl Pts',(-25.7650311139017,21.2091253362788,9.72906451135851));
#46400=CARTESIAN_POINT('Ctrl Pts',(-25.7637413077141,21.207905812741,9.7291746626015));
#46401=CARTESIAN_POINT('Ctrl Pts',(-25.7606622634242,21.2049993625376,9.72943721358092));
#46402=CARTESIAN_POINT('Ctrl Pts',(-25.7588720975974,21.2033134138709,9.72958953698752));
#46403=CARTESIAN_POINT('Ctrl Pts',(-25.7534613572047,21.1982293410369,9.73004895908232));
#46404=CARTESIAN_POINT('Ctrl Pts',(-25.749834835602,21.1948375136324,9.73035557275996));
#46405=CARTESIAN_POINT('Ctrl Pts',(-25.7130621182603,21.1606035706839,9.73345155269726));
#46406=CARTESIAN_POINT('Ctrl Pts',(-25.6792752501237,21.1304529032963,9.73618903330854));
#46407=CARTESIAN_POINT('Ctrl Pts',(-25.6419481672626,21.0985303548686,9.73911383187181));
#46408=CARTESIAN_POINT('Ctrl Pts',(-25.63902972821,21.0960434762595,9.73934186295353));
#46409=CARTESIAN_POINT('Ctrl Pts',(-25.6235770060692,21.0829233359351,9.74054588799739));
#46410=CARTESIAN_POINT('Ctrl Pts',(-25.6109657323873,21.0723806906732,9.74151683038013));
#46411=CARTESIAN_POINT('Ctrl Pts',(-25.5903853040761,21.055441872506,9.74308351228039));
#46412=CARTESIAN_POINT('Ctrl Pts',(-25.5824655700994,21.0489864273123,9.74368218509627));
#46413=CARTESIAN_POINT('Ctrl Pts',(-25.4988687441232,20.9815050604936,9.7499589079307));
#46414=CARTESIAN_POINT('Ctrl Pts',(-25.4204929068524,20.9238915367616,9.75547944982786));
#46415=CARTESIAN_POINT('Ctrl Pts',(-25.2669435169188,20.8213833328133,9.76586236129896));
#46416=CARTESIAN_POINT('Ctrl Pts',(-25.1923150816533,20.7758362065554,9.7707304264875));
#46417=CARTESIAN_POINT('Ctrl Pts',(-25.0372450068812,20.6896451844314,9.78065349991479));
#46418=CARTESIAN_POINT('Ctrl Pts',(-24.9567672916642,20.6492291977996,9.78570546873646));
#46419=CARTESIAN_POINT('Ctrl Pts',(-24.7716774881621,20.5657910055625,9.79726829109988));
#46420=CARTESIAN_POINT('Ctrl Pts',(-24.6662865639314,20.52480151575,9.80381544761824));
#46421=CARTESIAN_POINT('Ctrl Pts',(-24.511494706669,20.4737887367934,9.81352245850843));
#46422=CARTESIAN_POINT('Ctrl Pts',(-24.4636664800881,20.4592509892938,9.81653325743071));
#46423=CARTESIAN_POINT('Ctrl Pts',(-24.4078464421007,20.4436927416017,9.82006672093656));
#46424=CARTESIAN_POINT('Ctrl Pts',(-24.4001635701171,20.4415820329833,9.82055347659638));
#46425=CARTESIAN_POINT('Ctrl Pts',(-24.3884852046702,20.4384201749147,9.82129403789738));
#46426=CARTESIAN_POINT('Ctrl Pts',(-24.3844953477585,20.4373481717215,9.82154716509809));
#46427=CARTESIAN_POINT('Ctrl Pts',(-24.3772985949219,20.4354293628653,9.82200396321513));
#46428=CARTESIAN_POINT('Ctrl Pts',(-24.3740924269704,20.4345798289553,9.82220754519021));
#46429=CARTESIAN_POINT('Ctrl Pts',(-24.3676657890163,20.4328875850017,9.82261577479757));
#46430=CARTESIAN_POINT('Ctrl Pts',(-24.3644453134005,20.4320449122116,9.82282042336128));
#46431=CARTESIAN_POINT('Ctrl Pts',(-24.3554260847859,20.4296998571416,9.82339378456594));
#46432=CARTESIAN_POINT('Ctrl Pts',(-24.3496244622933,20.4282086561136,9.82376285920426));
#46433=CARTESIAN_POINT('Ctrl Pts',(-24.3260869767082,20.4222286847907,9.825261292322));
#46434=CARTESIAN_POINT('Ctrl Pts',(-24.3083174689608,20.4178748722262,9.82639500824015));
#46435=CARTESIAN_POINT('Ctrl Pts',(-24.0151418947004,20.348682935108,9.84514328749083));
#46436=CARTESIAN_POINT('Ctrl Pts',(-23.7324734711579,20.3202535138427,9.86401511527225));
#46437=CARTESIAN_POINT('Ctrl Pts',(-23.3181573708364,20.3331736238322,9.89207423456088));
#46438=CARTESIAN_POINT('Ctrl Pts',(-23.1868811615217,20.3453454307033,9.90099415660954));
#46439=CARTESIAN_POINT('Ctrl Pts',(-22.9772544214802,20.3778313754213,9.91498364404609));
#46440=CARTESIAN_POINT('Ctrl Pts',(-22.8982764789008,20.3931157567231,9.92019330915995));
#46441=CARTESIAN_POINT('Ctrl Pts',(-22.811789685451,20.4132379778774,9.9257711836903));
#46442=CARTESIAN_POINT('Ctrl Pts',(-22.8036408620733,20.4151674124913,9.92629546974006));
#46443=CARTESIAN_POINT('Ctrl Pts',(-22.7933033541201,20.4176576635031,9.92695888572668));
#46444=CARTESIAN_POINT('Ctrl Pts',(-22.7911077128188,20.4181890250432,9.92709969556467));
#46445=CARTESIAN_POINT('Ctrl Pts',(-22.7871674727165,20.4191469792042,9.92735221311207));
#46446=CARTESIAN_POINT('Ctrl Pts',(-22.7854226712723,20.4195727216987,9.92746396990977));
#46447=CARTESIAN_POINT('Ctrl Pts',(-22.7820396407255,20.4204011993433,9.9276805358768));
#46448=CARTESIAN_POINT('Ctrl Pts',(-22.7804013733479,20.420803761941,9.92778535477929));
#46449=CARTESIAN_POINT('Ctrl Pts',(-22.7769847458104,20.4216461566792,9.92800383995364));
#46450=CARTESIAN_POINT('Ctrl Pts',(-22.7752064494867,20.4220862175471,9.92811749239075));
#46451=CARTESIAN_POINT('Ctrl Pts',(-22.7702930072805,20.4233065550729,9.92843133643765));
#46452=CARTESIAN_POINT('Ctrl Pts',(-22.7671586469503,20.4240900329865,9.92863134174013));
#46453=CARTESIAN_POINT('Ctrl Pts',(-22.7548918589547,20.4271758972516,9.92941332558684));
#46454=CARTESIAN_POINT('Ctrl Pts',(-22.7457682457995,20.4295136282758,9.92999327312652));
#46455=CARTESIAN_POINT('Ctrl Pts',(-22.5919497870095,20.4696457137232,9.93974472504502));
#46456=CARTESIAN_POINT('Ctrl Pts',(-22.4500259417727,20.5174325613287,9.94835500180697));
#46457=CARTESIAN_POINT('Ctrl Pts',(-22.1607185321659,20.6378421865267,9.96605601923618));
#46458=CARTESIAN_POINT('Ctrl Pts',(-22.0145357699813,20.7122049266954,9.97509555538223));
#46459=CARTESIAN_POINT('Ctrl Pts',(-21.7569343781771,20.8690001841141,9.99212257320224));
#46460=CARTESIAN_POINT('Ctrl Pts',(-21.6439591265324,20.9481104005739,10.0000297559278));
#46461=CARTESIAN_POINT('Ctrl Pts',(-21.5072763004697,21.0575116246166,10.0104244143713));
#46462=CARTESIAN_POINT('Ctrl Pts',(-21.478560776641,21.0813251915461,10.0126578070469));
#46463=CARTESIAN_POINT('Ctrl Pts',(-21.4331613503375,21.1203243537113,10.0162735037541));
#46464=CARTESIAN_POINT('Ctrl Pts',(-21.4162117970594,21.1351963991918,10.0176429619218));
#46465=CARTESIAN_POINT('Ctrl Pts',(-21.3947564967531,21.1544241527385,10.0194022568126));
#46466=CARTESIAN_POINT('Ctrl Pts',(-21.3901051797319,21.1586170672071,10.0197852271972));
#46467=CARTESIAN_POINT('Ctrl Pts',(-21.3826809460276,21.1653489448089,10.0203990423436));
#46468=CARTESIAN_POINT('Ctrl Pts',(-21.3799001841313,21.167879264348,10.020629520337));
#46469=CARTESIAN_POINT('Ctrl Pts',(-21.3746449424871,21.1726780430055,10.0210661789662));
#46470=CARTESIAN_POINT('Ctrl Pts',(-21.3721695650827,21.1749455153488,10.0212723174305));
#46471=CARTESIAN_POINT('Ctrl Pts',(-21.366578574031,21.1800830117546,10.0217389529322));
#46472=CARTESIAN_POINT('Ctrl Pts',(-21.3634650716837,21.1829553152268,10.0219995471816));
#46473=CARTESIAN_POINT('Ctrl Pts',(-21.3554962380755,21.1903359497997,10.0226684173856));
#46474=CARTESIAN_POINT('Ctrl Pts',(-21.3506491480087,21.1948531143324,10.0230770720028));
#46475=CARTESIAN_POINT('Ctrl Pts',(-21.3259242485419,21.2180379486562,10.0251709403466));
#46476=CARTESIAN_POINT('Ctrl Pts',(-21.3062705046678,21.2369419686161,10.0268663471001));
#46477=CARTESIAN_POINT('Ctrl Pts',(-21.2802022522148,21.262660621387,10.0291578508912));
#46478=CARTESIAN_POINT('Ctrl Pts',(-21.2735736888501,21.2692574718488,10.0297443183353));
#46479=CARTESIAN_POINT('Ctrl Pts',(-21.2646534430799,21.2782126595186,10.0305387081105));
#46480=CARTESIAN_POINT('Ctrl Pts',(-21.2623364715423,21.2805458378238,10.0307455196922));
#46481=CARTESIAN_POINT('Ctrl Pts',(-21.2589751504957,21.2839410474797,10.0310462404424));
#46482=CARTESIAN_POINT('Ctrl Pts',(-21.2579279546272,21.2850002688243,10.0311400256239));
#46483=CARTESIAN_POINT('Ctrl Pts',(-21.254072397586,21.2889055125535,10.0314856837092));
#46484=CARTESIAN_POINT('Ctrl Pts',(-21.2512686080507,21.2917560256427,10.0317377545512));
#46485=CARTESIAN_POINT('Ctrl Pts',(-21.2435991667335,21.2995823537661,10.0324292052521));
#46486=CARTESIAN_POINT('Ctrl Pts',(-21.2387443373613,21.3045687021639,10.0328690490053));
#46487=CARTESIAN_POINT('Ctrl Pts',(-21.2295896692366,21.3140325117979,10.0337025414262));
#46488=CARTESIAN_POINT('Ctrl Pts',(-21.225286535791,21.3185067541449,10.034096047231));
#46489=CARTESIAN_POINT('Ctrl Pts',(-21.2149702038642,21.3292955209327,10.0350436024534));
#46490=CARTESIAN_POINT('Ctrl Pts',(-21.2089696767702,21.3356220466723,10.0355981783216));
#46491=CARTESIAN_POINT('Ctrl Pts',(-21.1841843416621,21.3619672442333,10.037903166935));
#46492=CARTESIAN_POINT('Ctrl Pts',(-21.1656304494669,21.3822007260568,10.0396629692902));
#46493=CARTESIAN_POINT('Ctrl Pts',(-21.0319835248743,21.5317371987251,10.0525935905876));
#46494=CARTESIAN_POINT('Ctrl Pts',(-20.9272300063733,21.6698743882735,10.0641562772667));
#46495=CARTESIAN_POINT('Ctrl Pts',(-20.7420943473768,21.959787700169,10.0874041577501));
#46496=CARTESIAN_POINT('Ctrl Pts',(-20.6617059540806,22.1109351431346,10.099046593302));
#46497=CARTESIAN_POINT('Ctrl Pts',(-20.5728105365335,22.3158670378401,10.1137209585626));
#46498=CARTESIAN_POINT('Ctrl Pts',(-20.5531149675324,22.3644888550931,10.1171239425134));
#46499=CARTESIAN_POINT('Ctrl Pts',(-20.5287398994178,22.4291564902782,10.12152786615));
#46500=CARTESIAN_POINT('Ctrl Pts',(-20.5229866617987,22.4447859780416,10.1225829862264));
#46501=CARTESIAN_POINT('Ctrl Pts',(-20.5138140375137,22.470313429217,10.1242904492873));
#46502=CARTESIAN_POINT('Ctrl Pts',(-20.510321354729,22.4801844775349,10.1249468613048));
#46503=CARTESIAN_POINT('Ctrl Pts',(-20.5058119972764,22.4931291370565,10.1258024872598));
#46504=CARTESIAN_POINT('Ctrl Pts',(-20.5047518092512,22.496187358702,10.1260042546633));
#46505=CARTESIAN_POINT('Ctrl Pts',(-20.5030272562966,22.5011863320313,10.1263334418329));
#46506=CARTESIAN_POINT('Ctrl Pts',(-20.5023601370619,22.5031261204637,10.1264610258994));
#46507=CARTESIAN_POINT('Ctrl Pts',(-20.5010830756246,22.5068510034069,10.126705724329));
#46508=CARTESIAN_POINT('Ctrl Pts',(-20.5004728505192,22.5086359912308,10.1268228551687));
#46509=CARTESIAN_POINT('Ctrl Pts',(-20.4990734541007,22.5127411799256,10.1270919399047));
#46510=CARTESIAN_POINT('Ctrl Pts',(-20.4982853599476,22.5150617515623,10.1272438292192));
#46511=CARTESIAN_POINT('Ctrl Pts',(-20.4957934779308,22.5224267679684,10.1277252090735));
#46512=CARTESIAN_POINT('Ctrl Pts',(-20.4940995323904,22.5274745706955,10.1280541155636));
#46513=CARTESIAN_POINT('Ctrl Pts',(-20.4798055621644,22.570421883641,10.1308440163167));
#46514=CARTESIAN_POINT('Ctrl Pts',(-20.4678978592618,22.6085504966277,10.1332648448311));
#46515=CARTESIAN_POINT('Ctrl Pts',(-20.4546015545916,22.6540836252423,10.136100511888));
#46516=CARTESIAN_POINT('Ctrl Pts',(-20.4525267711698,22.6612818935096,10.1365471700814));
#46517=CARTESIAN_POINT('Ctrl Pts',(-20.4435889773841,22.6927019991411,10.1384899805712));
#46518=CARTESIAN_POINT('Ctrl Pts',(-20.4369846504172,22.7169971539186,10.1399745578865));
#46519=CARTESIAN_POINT('Ctrl Pts',(-20.4176113813649,22.7917131184576,10.144493079108));
#46520=CARTESIAN_POINT('Ctrl Pts',(-20.4057773329277,22.8423692064602,10.1474913007309));
#46521=CARTESIAN_POINT('Ctrl Pts',(-20.3532243485018,23.0947567857408,10.162204494736));
#46522=CARTESIAN_POINT('Ctrl Pts',(-20.330666237766,23.2997810632507,10.1734794439604));
#46523=CARTESIAN_POINT('Ctrl Pts',(-20.3260243255975,23.6344957344806,10.1924330484611));
#46524=CARTESIAN_POINT('Ctrl Pts',(-20.3319759177558,23.7634073428135,10.1998575871149));
#46525=CARTESIAN_POINT('Ctrl Pts',(-20.3513725425805,23.9455017129285,10.2107420226139));
#46526=CARTESIAN_POINT('Ctrl Pts',(-20.3584716824424,23.9992398060966,10.2140028231158));
#46527=CARTESIAN_POINT('Ctrl Pts',(-20.3681891681188,24.0607976770839,10.2178024312092));
#46528=CARTESIAN_POINT('Ctrl Pts',(-20.3694865962945,24.068819458507,10.2182988261917));
#46529=CARTESIAN_POINT('Ctrl Pts',(-20.3714947908558,24.0809446553052,10.2190510751543));
#46530=CARTESIAN_POINT('Ctrl Pts',(-20.3721832017651,24.0850517827297,10.2193062174361));
#46531=CARTESIAN_POINT('Ctrl Pts',(-20.3733865518856,24.0921467104341,10.2197475514024));
#46532=CARTESIAN_POINT('Ctrl Pts',(-20.3738977513965,24.0951351467547,10.2199336237567));
#46533=CARTESIAN_POINT('Ctrl Pts',(-20.3749646707315,24.1013197570857,10.2203190759497));
#46534=CARTESIAN_POINT('Ctrl Pts',(-20.3755210009019,24.1045158212427,10.2205184750589));
#46535=CARTESIAN_POINT('Ctrl Pts',(-20.3768811670764,24.112260611558,10.2210021671578));
#46536=CARTESIAN_POINT('Ctrl Pts',(-20.3776899570954,24.1168084508386,10.221286617908));
#46537=CARTESIAN_POINT('Ctrl Pts',(-20.3807407659188,24.1337518074821,10.2223479420846));
#46538=CARTESIAN_POINT('Ctrl Pts',(-20.3830456534096,24.1461357594668,10.2231268197785));
#46539=CARTESIAN_POINT('Ctrl Pts',(-20.4236401278124,24.3573546845948,10.2364660490928));
#46540=CARTESIAN_POINT('Ctrl Pts',(-20.4805045395809,24.5521199163188,10.2496409639259));
#46541=CARTESIAN_POINT('Ctrl Pts',(-20.6644750750044,25.0151461744725,10.283006592554));
#46542=CARTESIAN_POINT('Ctrl Pts',(-20.8110326273105,25.2737115605248,10.30354247522));
#46543=CARTESIAN_POINT('Ctrl Pts',(-20.995608096444,25.5149336235747,10.322687537788));
#46544=CARTESIAN_POINT('Ctrl Pts',(-21.0004323161356,25.5211905963562,10.3231840236561));
#46545=CARTESIAN_POINT('Ctrl Pts',(-21.008836773015,25.5320086021746,10.3240421378804));
#46546=CARTESIAN_POINT('Ctrl Pts',(-21.0124063738628,25.5365777975498,10.3244044900252));
#46547=CARTESIAN_POINT('Ctrl Pts',(-21.0175760982318,25.5431585134001,10.324926202691));
#46548=CARTESIAN_POINT('Ctrl Pts',(-21.0191663008336,25.5451777585119,10.3250862646727));
#46549=CARTESIAN_POINT('Ctrl Pts',(-21.0219410934185,25.5486925416565,10.325364834075));
#46550=CARTESIAN_POINT('Ctrl Pts',(-21.023124597488,25.5501889323233,10.3254834196823));
#46551=CARTESIAN_POINT('Ctrl Pts',(-21.0254037608313,25.5530653915963,10.3257113461496));
#46552=CARTESIAN_POINT('Ctrl Pts',(-21.0264992210538,25.5544456098645,10.3258207010403));
#46553=CARTESIAN_POINT('Ctrl Pts',(-21.029095346845,25.5577110786939,10.3260793989734));
#46554=CARTESIAN_POINT('Ctrl Pts',(-21.0305969984067,25.5595955492751,10.3262286708006));
#46555=CARTESIAN_POINT('Ctrl Pts',(-21.0350771456954,25.5652049098675,10.3266729425233));
#46556=CARTESIAN_POINT('Ctrl Pts',(-21.0380618148502,25.5689248952871,10.3269675006466));
#46557=CARTESIAN_POINT('Ctrl Pts',(-21.0656660204678,25.6031737579567,10.3296788973547));
#46558=CARTESIAN_POINT('Ctrl Pts',(-21.0908340015717,25.6332591390837,10.3320568848884));
#46559=CARTESIAN_POINT('Ctrl Pts',(-21.1183446272352,25.6649508630178,10.3345670048003));
#46560=CARTESIAN_POINT('Ctrl Pts',(-21.1201456173546,25.6670202263773,10.3347309311805));
#46561=CARTESIAN_POINT('Ctrl Pts',(-21.1230447815097,25.6703428308316,10.3349941774349));
#46562=CARTESIAN_POINT('Ctrl Pts',(-21.124141285135,25.6715975197637,10.3350935949948));
#46563=CARTESIAN_POINT('Ctrl Pts',(-21.1324227555589,25.6810588835894,10.3358433635224));
#46564=CARTESIAN_POINT('Ctrl Pts',(-21.1396484600537,25.6892299863481,10.3364913404259));
#46565=CARTESIAN_POINT('Ctrl Pts',(-21.1524203672679,25.7035260262691,10.337626160937));
#46566=CARTESIAN_POINT('Ctrl Pts',(-21.1579488588396,25.7096665657605,10.3381139678288));
#46567=CARTESIAN_POINT('Ctrl Pts',(-21.1869951468207,25.7416800534615,10.3406594965129));
#46568=CARTESIAN_POINT('Ctrl Pts',(-21.2109099658353,25.7671910899603,10.3426961197103));
#46569=CARTESIAN_POINT('Ctrl Pts',(-21.4324401971319,25.9959302983987,10.3610868640007));
#46570=CARTESIAN_POINT('Ctrl Pts',(-21.6556512693953,26.1726516140465,10.3763583019341));
#46571=CARTESIAN_POINT('Ctrl Pts',(-21.9567406782508,26.3522767329498,10.3965290944547));
#46572=CARTESIAN_POINT('Ctrl Pts',(-22.0154087963457,26.3848371833493,10.4004350448422));
#46573=CARTESIAN_POINT('Ctrl Pts',(-22.0750360597002,26.4155367973924,10.4044010236784));
#46574=CARTESIAN_POINT('Origin',(-23.5502525316942,23.5502525316942,-77.3107734492734));
#46575=CARTESIAN_POINT('',(-22.075036015346,26.4155367745563,11.9036974267447));
#46576=CARTESIAN_POINT('',(-22.0750360887345,26.4155368123409,11.6559056162233));
#46577=CARTESIAN_POINT('',(-22.0750360153461,26.4155367745563,-77.3107734492734));
#46578=CARTESIAN_POINT('',(-26.7730011657502,23.5472853461167,11.0607734492729));
#46579=CARTESIAN_POINT('Ctrl Pts',(-26.7730011657502,23.5472853461167,11.0607734492729));
#46580=CARTESIAN_POINT('Ctrl Pts',(-26.7728766101578,23.412001807288,11.0691292856908));
#46581=CARTESIAN_POINT('Ctrl Pts',(-26.7642301502994,23.2770954679651,11.0774851221087));
#46582=CARTESIAN_POINT('Ctrl Pts',(-26.7472248682243,23.143453512569,11.0858409585267));
#46583=CARTESIAN_POINT('Ctrl Pts',(-26.7337234486191,23.0373478855828,11.0924751121462));
#46584=CARTESIAN_POINT('Ctrl Pts',(-26.7149538773761,22.9320384752182,11.0991092657658));
#46585=CARTESIAN_POINT('Ctrl Pts',(-26.6910180747066,22.8279580167446,11.1057434193854));
#46586=CARTESIAN_POINT('Ctrl Pts',(-26.6687493772687,22.7311266603478,11.1119155106977));
#46587=CARTESIAN_POINT('Ctrl Pts',(-26.6419592261036,22.6351555609155,11.1180876020101));
#46588=CARTESIAN_POINT('Ctrl Pts',(-26.6107288815254,22.5404990594922,11.1242596933224));
#46589=CARTESIAN_POINT('Ctrl Pts',(-26.5795408509766,22.4459708082704,11.1304234220612));
#46590=CARTESIAN_POINT('Ctrl Pts',(-26.5439247194081,22.352754023724,11.1365871508));
#46591=CARTESIAN_POINT('Ctrl Pts',(-26.5040125621126,22.2612920027397,11.1427508795388));
#46592=CARTESIAN_POINT('Ctrl Pts',(-26.4641426880019,22.1699268771826,11.1489080783854));
#46593=CARTESIAN_POINT('Ctrl Pts',(-26.4199860092171,22.0803132152584,11.1550652772321));
#46594=CARTESIAN_POINT('Ctrl Pts',(-26.3717238173773,21.992877385313,11.1612224760788));
#46595=CARTESIAN_POINT('Ctrl Pts',(-26.3234969022729,21.9055054656569,11.1673751743865));
#46596=CARTESIAN_POINT('Ctrl Pts',(-26.2711706496585,21.8203085922524,11.1735278726942));
#46597=CARTESIAN_POINT('Ctrl Pts',(-26.2149733013765,21.7376905928564,11.1796805710019));
#46598=CARTESIAN_POINT('Ctrl Pts',(-26.158797263209,21.6551039223233,11.1858309361976));
#46599=CARTESIAN_POINT('Ctrl Pts',(-26.0987532901732,21.5750945414807,11.1919813013934));
#46600=CARTESIAN_POINT('Ctrl Pts',(-26.0351136844878,21.4980384556687,11.1981316665891));
#46601=CARTESIAN_POINT('Ctrl Pts',(-25.971481185564,21.4209909748634,11.2042813449613));
#46602=CARTESIAN_POINT('Ctrl Pts',(-25.9042541289125,21.3468964683414,11.2104310233336));
#46603=CARTESIAN_POINT('Ctrl Pts',(-25.8337453125777,21.2760981213357,11.2165807017058));
#46604=CARTESIAN_POINT('Ctrl Pts',(-25.7632255070671,21.2052887400292,11.2227313385382));
#46605=CARTESIAN_POINT('Ctrl Pts',(-25.6894232325111,21.1377768464531,11.2288819753707));
#46606=CARTESIAN_POINT('Ctrl Pts',(-25.6126876401643,21.0738682751924,11.2350326122031));
#46607=CARTESIAN_POINT('Ctrl Pts',(-25.5358699568532,21.0098913351855,11.2411898289249));
#46608=CARTESIAN_POINT('Ctrl Pts',(-25.4561130238567,20.949525693689,11.2473470456467));
#46609=CARTESIAN_POINT('Ctrl Pts',(-25.373798434421,20.8930363374133,11.2535042623686));
#46610=CARTESIAN_POINT('Ctrl Pts',(-25.2914379220129,20.8365154659572,11.2596649141764));
#46611=CARTESIAN_POINT('Ctrl Pts',(-25.2065172807383,20.7838754153129,11.2658255659842));
#46612=CARTESIAN_POINT('Ctrl Pts',(-25.1194445925097,20.735336220545,11.271986217792));
#46613=CARTESIAN_POINT('Ctrl Pts',(-25.0322262007103,20.6867158024436,11.278157178561));
#46614=CARTESIAN_POINT('Ctrl Pts',(-24.9428489578115,20.6422101410048,11.2843281393301));
#46615=CARTESIAN_POINT('Ctrl Pts',(-24.8517430197356,20.6019920153833,11.2904991000991));
#46616=CARTESIAN_POINT('Ctrl Pts',(-24.7822001466058,20.5712927649647,11.2952095103195));
#46617=CARTESIAN_POINT('Ctrl Pts',(-24.7116504972118,20.5430906941663,11.2999199205399));
#46618=CARTESIAN_POINT('Ctrl Pts',(-24.6402909599315,20.5174429782494,11.3046303307602));
#46619=CARTESIAN_POINT('Ctrl Pts',(-24.5467879401322,20.4838365539285,11.3108024220726));
#46620=CARTESIAN_POINT('Ctrl Pts',(-24.4515646315331,20.4544991098487,11.3169745133849));
#46621=CARTESIAN_POINT('Ctrl Pts',(-24.3550472035227,20.4296078709396,11.3231466046972));
#46622=CARTESIAN_POINT('Ctrl Pts',(-24.2586605470852,20.4047503571983,11.329310333436));
#46623=CARTESIAN_POINT('Ctrl Pts',(-24.1609836732443,20.3843271824758,11.3354740621748));
#46624=CARTESIAN_POINT('Ctrl Pts',(-24.062460927403,20.3684668503722,11.3416377909136));
#46625=CARTESIAN_POINT('Ctrl Pts',(-23.9640425571641,20.352623320802,11.3477949897603));
#46626=CARTESIAN_POINT('Ctrl Pts',(-23.8647805230092,20.3413330922724,11.353952188607));
#46627=CARTESIAN_POINT('Ctrl Pts',(-23.765131531587,20.3346741112689,11.3601093874537));
#46628=CARTESIAN_POINT('Ctrl Pts',(-23.6655553775348,20.3280199975766,11.3662620857614));
#46629=CARTESIAN_POINT('Ctrl Pts',(-23.56559326068,20.3259904300169,11.3724147840691));
#46630=CARTESIAN_POINT('Ctrl Pts',(-23.4657083024818,20.3286116709205,11.3785674823768));
#46631=CARTESIAN_POINT('Ctrl Pts',(-23.3658612208019,20.3312319178457,11.3847178475726));
#46632=CARTESIAN_POINT('Ctrl Pts',(-23.2660916734112,20.3384994576095,11.3908682127683));
#46633=CARTESIAN_POINT('Ctrl Pts',(-23.1668631908042,20.350388444613,11.3970185779641));
#46634=CARTESIAN_POINT('Ctrl Pts',(-23.0676457892397,20.3622761039496,11.4031682563363));
#46635=CARTESIAN_POINT('Ctrl Pts',(-22.9689697636495,20.3787841327985,11.4093179347085));
#46636=CARTESIAN_POINT('Ctrl Pts',(-22.8712929221316,20.3998348750838,11.4154676130807));
#46637=CARTESIAN_POINT('Ctrl Pts',(-22.7736008571558,20.4208888982398,11.4216182499132));
#46638=CARTESIAN_POINT('Ctrl Pts',(-22.6769087102609,20.4464869495863,11.4277688867456));
#46639=CARTESIAN_POINT('Ctrl Pts',(-22.5816625162692,20.4765005988735,11.4339195235781));
#46640=CARTESIAN_POINT('Ctrl Pts',(-22.4863144288581,20.5065463564606,11.4400767402999));
#46641=CARTESIAN_POINT('Ctrl Pts',(-22.3924157984164,20.541017014062,11.4462339570217));
#46642=CARTESIAN_POINT('Ctrl Pts',(-22.3003958300361,20.5797347674281,11.4523911737436));
#46643=CARTESIAN_POINT('Ctrl Pts',(-22.2083245240924,20.6184741212702,11.4585518255514));
#46644=CARTESIAN_POINT('Ctrl Pts',(-22.1181343596272,20.6614651026508,11.4647124773592));
#46645=CARTESIAN_POINT('Ctrl Pts',(-22.0302310414056,20.70848332369,11.470873129167));
#46646=CARTESIAN_POINT('Ctrl Pts',(-21.9421806296738,20.755580222933,11.477044089936));
#46647=CARTESIAN_POINT('Ctrl Pts',(-21.8564250812213,20.8067176002407,11.4832150507051));
#46648=CARTESIAN_POINT('Ctrl Pts',(-21.7733422755615,20.8616269526761,11.4893860114741));
#46649=CARTESIAN_POINT('Ctrl Pts',(-21.7099236100468,20.9035402923627,11.4940964216945));
#46650=CARTESIAN_POINT('Ctrl Pts',(-21.6480616583938,20.9476504812598,11.4988068319148));
#46651=CARTESIAN_POINT('Ctrl Pts',(-21.587910949624,20.9938227795245,11.5035172421352));
#46652=CARTESIAN_POINT('Ctrl Pts',(-21.5090949549101,21.0543227418755,11.5096893334475));
#46653=CARTESIAN_POINT('Ctrl Pts',(-21.4329406358746,21.1185775768524,11.5158614247599));
#46654=CARTESIAN_POINT('Ctrl Pts',(-21.3598274574452,21.1863245385859,11.5220335160722));
#46655=CARTESIAN_POINT('Ctrl Pts',(-21.2868133401444,21.2539797098838,11.528197244811));
#46656=CARTESIAN_POINT('Ctrl Pts',(-21.2168324894578,21.3251173109555,11.5343609735497));
#46657=CARTESIAN_POINT('Ctrl Pts',(-21.1502332051477,21.3994329682014,11.5405247022885));
#46658=CARTESIAN_POINT('Ctrl Pts',(-21.0837044765288,21.4736698949833,11.5466819011352));
#46659=CARTESIAN_POINT('Ctrl Pts',(-21.0205504803597,21.5510778626136,11.5528390999819));
#46660=CARTESIAN_POINT('Ctrl Pts',(-20.9610836636312,21.6313147695056,11.5589962988285));
#46661=CARTESIAN_POINT('Ctrl Pts',(-20.9016603135395,21.7114930280845,11.5651489971362));
#46662=CARTESIAN_POINT('Ctrl Pts',(-20.845919042444,21.794495766878,11.5713016954439));
#46663=CARTESIAN_POINT('Ctrl Pts',(-20.7941322820659,21.8799475499352,11.5774543937516));
#46664=CARTESIAN_POINT('Ctrl Pts',(-20.742365159301,21.9653669295547,11.5836047589474));
#46665=CARTESIAN_POINT('Ctrl Pts',(-20.6945497925449,22.0532331370677,11.5897551241432));
#46666=CARTESIAN_POINT('Ctrl Pts',(-20.6509149953443,22.1431422258502,11.5959054893389));
#46667=CARTESIAN_POINT('Ctrl Pts',(-20.6072850709284,22.2330412743055,11.6020551677111));
#46668=CARTESIAN_POINT('Ctrl Pts',(-20.5678349775696,22.3249823596631,11.6082048460833));
#46669=CARTESIAN_POINT('Ctrl Pts',(-20.5327468465931,22.4185383438878,11.6143545244555));
#46670=CARTESIAN_POINT('Ctrl Pts',(-20.4976532469438,22.5121089093126,11.620505161288));
#46671=CARTESIAN_POINT('Ctrl Pts',(-20.4669231125643,22.6072944667511,11.6266557981204));
#46672=CARTESIAN_POINT('Ctrl Pts',(-20.4406894936607,22.703650337629,11.6328064349529));
#46673=CARTESIAN_POINT('Ctrl Pts',(-20.4144278102958,22.8001092890476,11.6389636516747));
#46674=CARTESIAN_POINT('Ctrl Pts',(-20.3926723624938,22.897740634041,11.6451208683965));
#46675=CARTESIAN_POINT('Ctrl Pts',(-20.3755055641038,22.9960871644295,11.6512780851183));
#46676=CARTESIAN_POINT('Ctrl Pts',(-20.3583291884273,23.0944885619444,11.6574387369261));
#46677=CARTESIAN_POINT('Ctrl Pts',(-20.3457466150501,23.1936055084951,11.6635993887339));
#46678=CARTESIAN_POINT('Ctrl Pts',(-20.3377883633087,23.2929753866941,11.6697600405417));
#46679=CARTESIAN_POINT('Ctrl Pts',(-20.3298167945822,23.3925115460356,11.6759310013108));
#46680=CARTESIAN_POINT('Ctrl Pts',(-20.3264850187324,23.4923010480786,11.6821019620798));
#46681=CARTESIAN_POINT('Ctrl Pts',(-20.3277713996297,23.591880839228,11.6882729228488));
#46682=CARTESIAN_POINT('Ctrl Pts',(-20.3287533183215,23.6678919635137,11.6929833330692));
#46683=CARTESIAN_POINT('Ctrl Pts',(-20.3324249529497,23.743780888438,11.6976937432897));
#46684=CARTESIAN_POINT('Ctrl Pts',(-20.3387564741105,23.8193447735452,11.7024041535101));
#46685=CARTESIAN_POINT('Ctrl Pts',(-20.3470527211297,23.9183567867183,11.7085762448224));
#46686=CARTESIAN_POINT('Ctrl Pts',(-20.3599467540298,24.0171591553197,11.7147483361347));
#46687=CARTESIAN_POINT('Ctrl Pts',(-20.3774226371827,24.1152906038577,11.720920427447));
#46688=CARTESIAN_POINT('Ctrl Pts',(-20.3948748422417,24.2132890939845,11.7270841561858));
#46689=CARTESIAN_POINT('Ctrl Pts',(-20.4168964830926,24.3106180469394,11.7332478849246));
#46690=CARTESIAN_POINT('Ctrl Pts',(-20.4434197559064,24.4068199054544,11.7394116136634));
#46691=CARTESIAN_POINT('Ctrl Pts',(-20.4699149298019,24.5029198471293,11.7455688125101));
#46692=CARTESIAN_POINT('Ctrl Pts',(-20.500902139522,24.5978946517805,11.7517260113567));
#46693=CARTESIAN_POINT('Ctrl Pts',(-20.5362624601059,24.6912965321022,11.7578832102034));
#46694=CARTESIAN_POINT('Ctrl Pts',(-20.5715969344397,24.7846301413135,11.7640359085111));
#46695=CARTESIAN_POINT('Ctrl Pts',(-20.6112980111599,24.8763927069807,11.7701886068188));
#46696=CARTESIAN_POINT('Ctrl Pts',(-20.6551970905961,24.9661520886785,11.7763413051265));
#46697=CARTESIAN_POINT('Ctrl Pts',(-20.699079523439,25.0558774334911,11.7824916703223));
#46698=CARTESIAN_POINT('Ctrl Pts',(-20.7471566052917,25.1436007138747,11.788642035518));
#46699=CARTESIAN_POINT('Ctrl Pts',(-20.799212172504,25.2289110748788,11.7947924007138));
#46700=CARTESIAN_POINT('Ctrl Pts',(-20.8512619265674,25.3142119091048,11.800942079086));
#46701=CARTESIAN_POINT('Ctrl Pts',(-20.9072890564203,25.397099988846,11.8070917574582));
#46702=CARTESIAN_POINT('Ctrl Pts',(-20.9670326533697,25.477191197747,11.8132414358304));
#46703=CARTESIAN_POINT('Ctrl Pts',(-21.026785561678,25.5572948892909,11.8193920726629));
#46704=CARTESIAN_POINT('Ctrl Pts',(-21.0902558278228,25.6346004959399,11.8255427094953));
#46705=CARTESIAN_POINT('Ctrl Pts',(-21.1571412555356,25.7087557127024,11.8316933463278));
#46706=CARTESIAN_POINT('Ctrl Pts',(-21.2240982366056,25.7829902599693,11.8378505630496));
#46707=CARTESIAN_POINT('Ctrl Pts',(-21.2944773834156,25.8540673640787,11.8440077797714));
#46708=CARTESIAN_POINT('Ctrl Pts',(-21.3679385872317,25.9216705484733,11.8501649964932));
#46709=CARTESIAN_POINT('Ctrl Pts',(-21.4414407747526,25.9893114484076,11.8563256483011));
#46710=CARTESIAN_POINT('Ctrl Pts',(-21.5180281105708,26.0534742899796,11.8624863001088));
#46711=CARTESIAN_POINT('Ctrl Pts',(-21.5973278839115,26.1138833324498,11.8686469519166));
#46712=CARTESIAN_POINT('Ctrl Pts',(-21.6767603539723,26.1743934607297,11.8748179126857));
#46713=CARTESIAN_POINT('Ctrl Pts',(-21.7589139702431,26.231136995885,11.8809888734547));
#46714=CARTESIAN_POINT('Ctrl Pts',(-21.84338746272,26.2838818406561,11.8871598342238));
#46715=CARTESIAN_POINT('Ctrl Pts',(-21.9078676655937,26.3241429710021,11.8918702444441));
#46716=CARTESIAN_POINT('Ctrl Pts',(-21.9736989655831,26.3620751442669,11.8965806546645));
#46717=CARTESIAN_POINT('Ctrl Pts',(-22.0406945855522,26.397593812563,11.9012910648848));
#46718=CARTESIAN_POINT('Ctrl Pts',(-22.0521030543927,26.4036421724513,11.9020931855048));
#46719=CARTESIAN_POINT('Ctrl Pts',(-22.0635504782946,26.4096233458974,11.9028953061248));
#46720=CARTESIAN_POINT('Ctrl Pts',(-22.075036015346,26.4155367745563,11.9036974267448));
#46721=CARTESIAN_POINT('Ctrl Pts',(-26.7730011593802,23.5472784355037,11.0606497612747));
#46722=CARTESIAN_POINT('Ctrl Pts',(-26.7732128984034,23.7767201223076,11.0478295799405));
#46723=CARTESIAN_POINT('Ctrl Pts',(-26.7489235004643,24.0055091845135,11.034997470879));
#46724=CARTESIAN_POINT('Ctrl Pts',(-26.690296845201,24.2773033895601,11.0184510144448));
#46725=CARTESIAN_POINT('Ctrl Pts',(-26.6789720184836,24.324587875792,11.0155259372985));
#46726=CARTESIAN_POINT('Ctrl Pts',(-26.6648259122225,24.3782608176138,11.0121464884727));
#46727=CARTESIAN_POINT('Ctrl Pts',(-26.6630480283088,24.3849196865192,11.0117261762637));
#46728=CARTESIAN_POINT('Ctrl Pts',(-26.6601112650086,24.3957791183713,11.0110389954556));
#46729=CARTESIAN_POINT('Ctrl Pts',(-26.6589651959815,24.3999831481575,11.0107725428983));
#46730=CARTESIAN_POINT('Ctrl Pts',(-26.6567254242061,24.4081339359079,11.0102551170065));
#46731=CARTESIAN_POINT('Ctrl Pts',(-26.6556327168615,24.4120809606345,11.0100041764616));
#46732=CARTESIAN_POINT('Ctrl Pts',(-26.6537202984865,24.4189380463477,11.0095675635285));
#46733=CARTESIAN_POINT('Ctrl Pts',(-26.6529040089133,24.4218490631799,11.0093820029019));
#46734=CARTESIAN_POINT('Ctrl Pts',(-26.6511948878978,24.4279112312635,11.008995141789));
#46735=CARTESIAN_POINT('Ctrl Pts',(-26.6503013470046,24.4310621774152,11.0087938183256));
#46736=CARTESIAN_POINT('Ctrl Pts',(-26.647833162831,24.439715601717,11.0082402517437));
#46737=CARTESIAN_POINT('Ctrl Pts',(-26.6462486680147,24.4452152362473,11.0078876870998));
#46738=CARTESIAN_POINT('Ctrl Pts',(-26.6400779124813,24.4664208517994,11.0065253484169));
#46739=CARTESIAN_POINT('Ctrl Pts',(-26.6353867795628,24.4820958292839,11.005512147522));
#46740=CARTESIAN_POINT('Ctrl Pts',(-26.5530367622513,24.7498210546617,10.9880990312428));
#46741=CARTESIAN_POINT('Ctrl Pts',(-26.4448630840975,24.9913800011566,10.9706198347406));
#46742=CARTESIAN_POINT('Ctrl Pts',(-26.2859366488993,25.2543816848082,10.9498369250046));
#46743=CARTESIAN_POINT('Ctrl Pts',(-26.2625992944151,25.2912863593656,10.9468798659495));
#46744=CARTESIAN_POINT('Ctrl Pts',(-26.2156247034077,25.3623319768872,10.9411172406081));
#46745=CARTESIAN_POINT('Ctrl Pts',(-26.1920628593873,25.3965133464821,10.9383118960035));
#46746=CARTESIAN_POINT('Ctrl Pts',(-26.1049184440959,25.5178492167718,10.9282535880205));
#46747=CARTESIAN_POINT('Ctrl Pts',(-26.0376245589581,25.6022610579256,10.9210639760687));
#46748=CARTESIAN_POINT('Ctrl Pts',(-25.9361708697199,25.717179493118,10.9111594728993));
#46749=CARTESIAN_POINT('Ctrl Pts',(-25.9054058935783,25.7505779493756,10.9082661362026));
#46750=CARTESIAN_POINT('Ctrl Pts',(-25.8715133164393,25.7858460172218,10.9052053112538));
#46751=CARTESIAN_POINT('Ctrl Pts',(-25.8690789771374,25.7883708885998,10.9049861532107));
#46752=CARTESIAN_POINT('Ctrl Pts',(-25.8650516983214,25.7925343165894,10.9046247255665));
#46753=CARTESIAN_POINT('Ctrl Pts',(-25.8634611368485,25.7941751537577,10.9044822731369));
#46754=CARTESIAN_POINT('Ctrl Pts',(-25.8603536307343,25.797374068994,10.9042045338914));
#46755=CARTESIAN_POINT('Ctrl Pts',(-25.8588368522113,25.7989323057644,10.9040692342311));
#46756=CARTESIAN_POINT('Ctrl Pts',(-25.8561476054347,25.8016894691796,10.9038298194651));
#46757=CARTESIAN_POINT('Ctrl Pts',(-25.8549757850054,25.8028890093015,10.9037256544237));
#46758=CARTESIAN_POINT('Ctrl Pts',(-25.8524642776507,25.8054559157993,10.9035027408083));
#46759=CARTESIAN_POINT('Ctrl Pts',(-25.851124312352,25.8068229994438,10.9033840151966));
#46760=CARTESIAN_POINT('Ctrl Pts',(-25.8472330178103,25.8107859768783,10.90303982583));
#46761=CARTESIAN_POINT('Ctrl Pts',(-25.8446784973827,25.8133787541306,10.9028146137892));
#46762=CARTESIAN_POINT('Ctrl Pts',(-25.8331698918202,25.8250201995503,10.9018032732035));
#46763=CARTESIAN_POINT('Ctrl Pts',(-25.8241664720607,25.8340202564006,10.9010209941633));
#46764=CARTESIAN_POINT('Ctrl Pts',(-25.6686950401911,25.9876026669407,10.8876595817541));
#46765=CARTESIAN_POINT('Ctrl Pts',(-25.5087362051239,26.11790594733,10.8761215485457));
#46766=CARTESIAN_POINT('Ctrl Pts',(-25.2618465006103,26.282433071645,10.8595336611637));
#46767=CARTESIAN_POINT('Ctrl Pts',(-25.1841826202237,26.3295755775236,10.8544722590818));
#46768=CARTESIAN_POINT('Ctrl Pts',(-25.0053737376604,26.4280257865806,10.8429795710441));
#46769=CARTESIAN_POINT('Ctrl Pts',(-24.9033078126986,26.4774004814728,10.8365261831315));
#46770=CARTESIAN_POINT('Ctrl Pts',(-24.7415250626844,26.5453911254332,10.8262745970161));
#46771=CARTESIAN_POINT('Ctrl Pts',(-24.6835077975662,26.5678206243763,10.8225947878011));
#46772=CARTESIAN_POINT('Ctrl Pts',(-24.5935901079937,26.5996239168669,10.8168658955509));
#46773=CARTESIAN_POINT('Ctrl Pts',(-24.5621314372683,26.6102067955271,10.814856922907));
#46774=CARTESIAN_POINT('Ctrl Pts',(-24.5256591787038,26.621852347267,10.8125207108932));
#46775=CARTESIAN_POINT('Ctrl Pts',(-24.5207988998445,26.6233915296662,10.8122092450651));
#46776=CARTESIAN_POINT('Ctrl Pts',(-24.5115171479648,26.6263067156798,10.8116141520718));
#46777=CARTESIAN_POINT('Ctrl Pts',(-24.5070963177831,26.6276847363053,10.8113305919417));
#46778=CARTESIAN_POINT('Ctrl Pts',(-24.4994114225286,26.6300620412473,10.8108374516701));
#46779=CARTESIAN_POINT('Ctrl Pts',(-24.4961487031162,26.6310656788889,10.8106280148865));
#46780=CARTESIAN_POINT('Ctrl Pts',(-24.489866913102,26.6329870862517,10.8102246483926));
#46781=CARTESIAN_POINT('Ctrl Pts',(-24.4868480754787,26.6339056099207,10.81003074369));
#46782=CARTESIAN_POINT('Ctrl Pts',(-24.4797253601243,26.6360613715805,10.80957309905));
#46783=CARTESIAN_POINT('Ctrl Pts',(-24.4756203604392,26.6372948566969,10.8093092363698));
#46784=CARTESIAN_POINT('Ctrl Pts',(-24.4613798131291,26.6415429510651,10.80839348592));
#46785=CARTESIAN_POINT('Ctrl Pts',(-24.4512319810967,26.6445158377725,10.8077402341967));
#46786=CARTESIAN_POINT('Ctrl Pts',(-24.3300943885958,26.6793576112831,10.7999336184134));
#46787=CARTESIAN_POINT('Ctrl Pts',(-24.2174967936964,26.7052852637205,10.7925871131172));
#46788=CARTESIAN_POINT('Ctrl Pts',(-23.9625125640323,26.7497395096324,10.7757259857807));
#46789=CARTESIAN_POINT('Ctrl Pts',(-23.8197909062603,26.7649091401567,10.7661317973485));
#46790=CARTESIAN_POINT('Ctrl Pts',(-23.525300221796,26.7764586014372,10.746220511709));
#46791=CARTESIAN_POINT('Ctrl Pts',(-23.3738203884374,26.7717277280065,10.7359171482124));
#46792=CARTESIAN_POINT('Ctrl Pts',(-23.131986108612,26.7470607773478,10.7197917188221));
#46793=CARTESIAN_POINT('Ctrl Pts',(-23.0411702309593,26.7338618894257,10.7138135731468));
#46794=CARTESIAN_POINT('Ctrl Pts',(-22.9403154489346,26.7147767114425,10.7073497356995));
#46795=CARTESIAN_POINT('Ctrl Pts',(-22.9296086440722,26.7126942627053,10.7066657726361));
#46796=CARTESIAN_POINT('Ctrl Pts',(-22.9165103107795,26.7100775838797,10.7058319572611));
#46797=CARTESIAN_POINT('Ctrl Pts',(-22.9141087236917,26.7095949662245,10.7056791971631));
#46798=CARTESIAN_POINT('Ctrl Pts',(-22.9094608704415,26.7086554293309,10.705383792935));
#46799=CARTESIAN_POINT('Ctrl Pts',(-22.9072145379669,26.7081988510025,10.7052411294067));
#46800=CARTESIAN_POINT('Ctrl Pts',(-22.9031416539365,26.7073664909693,10.7049826587916));
#46801=CARTESIAN_POINT('Ctrl Pts',(-22.9013149473845,26.7069915218049,10.7048668054145));
#46802=CARTESIAN_POINT('Ctrl Pts',(-22.8976392891047,26.7062336918469,10.7046338325853));
#46803=CARTESIAN_POINT('Ctrl Pts',(-22.8957903558574,26.7058507932106,10.7045167158806));
#46804=CARTESIAN_POINT('Ctrl Pts',(-22.890505250952,26.7047514473032,10.7041821497165));
#46805=CARTESIAN_POINT('Ctrl Pts',(-22.8870698982306,26.7040310080581,10.7039649303278));
#46806=CARTESIAN_POINT('Ctrl Pts',(-22.8722933418599,26.7009069556398,10.703031652652));
#46807=CARTESIAN_POINT('Ctrl Pts',(-22.8609637921499,26.6984477298026,10.7023187554815));
#46808=CARTESIAN_POINT('Ctrl Pts',(-22.6664534247087,26.6551263638781,10.6901215307164));
#46809=CARTESIAN_POINT('Ctrl Pts',(-22.4871424159341,26.5983932464084,10.6795096899166));
#46810=CARTESIAN_POINT('Ctrl Pts',(-22.2326864821954,26.4926743659886,10.6640744991824));
#46811=CARTESIAN_POINT('Ctrl Pts',(-22.1530436379315,26.4556996817807,10.6591872317164));
#46812=CARTESIAN_POINT('Ctrl Pts',(-22.0750358939633,26.4155367120613,10.654266819213));
#46813=CARTESIAN_POINT('Ctrl Pts',(-22.0750360597002,26.4155367973924,10.4044010236784));
#46814=CARTESIAN_POINT('Ctrl Pts',(-22.1193205426974,26.4383370478085,10.4073465105658));
#46815=CARTESIAN_POINT('Ctrl Pts',(-22.1641340840807,26.4601108885803,10.4103249860603));
#46816=CARTESIAN_POINT('Ctrl Pts',(-22.2272148220196,26.4889717770413,10.4145229535466));
#46817=CARTESIAN_POINT('Ctrl Pts',(-22.2450615811766,26.4969415449219,10.4157112079245));
#46818=CARTESIAN_POINT('Ctrl Pts',(-22.2684346000349,26.5071251634973,10.4172685149745));
#46819=CARTESIAN_POINT('Ctrl Pts',(-22.2738963127654,26.5094868536566,10.4176324983703));
#46820=CARTESIAN_POINT('Ctrl Pts',(-22.282755360233,26.5132884913216,10.4182230275066));
#46821=CARTESIAN_POINT('Ctrl Pts',(-22.2861486995844,26.5147377617422,10.4184492545082));
#46822=CARTESIAN_POINT('Ctrl Pts',(-22.2926480336091,26.5175003914179,10.41888261756));
#46823=CARTESIAN_POINT('Ctrl Pts',(-22.2957536172038,26.5188147102654,10.4190897205461));
#46824=CARTESIAN_POINT('Ctrl Pts',(-22.3028164643854,26.5217907262478,10.4195607905982));
#46825=CARTESIAN_POINT('Ctrl Pts',(-22.3067749900918,26.5234493948298,10.419824860338));
#46826=CARTESIAN_POINT('Ctrl Pts',(-22.3171607582342,26.5277767838768,10.4205178185527));
#46827=CARTESIAN_POINT('Ctrl Pts',(-22.3235933266464,26.5304325912819,10.4209471449073));
#46828=CARTESIAN_POINT('Ctrl Pts',(-22.3563854140118,26.5438472681685,10.4231364998463));
#46829=CARTESIAN_POINT('Ctrl Pts',(-22.3828774004522,26.5542770588902,10.4249076292453));
#46830=CARTESIAN_POINT('Ctrl Pts',(-22.4159562274997,26.5667964249225,10.4271227406175));
#46831=CARTESIAN_POINT('Ctrl Pts',(-22.4224168149728,26.5692178776985,10.4275555406217));
#46832=CARTESIAN_POINT('Ctrl Pts',(-22.435254856928,26.5739826636259,10.4284159179758));
#46833=CARTESIAN_POINT('Ctrl Pts',(-22.4416320463025,26.576326612697,10.4288434722868));
#46834=CARTESIAN_POINT('Ctrl Pts',(-22.4499557401983,26.579356160111,10.4294017549609));
#46835=CARTESIAN_POINT('Ctrl Pts',(-22.451895593106,26.5800600926604,10.4295318798039));
#46836=CARTESIAN_POINT('Ctrl Pts',(-22.4562297950958,26.5816281755203,10.4298226529442));
#46837=CARTESIAN_POINT('Ctrl Pts',(-22.458624492687,26.5824913525278,10.4299833330185));
#46838=CARTESIAN_POINT('Ctrl Pts',(-22.4675138354534,26.5856836515596,10.4305798841966));
#46839=CARTESIAN_POINT('Ctrl Pts',(-22.4740148972478,26.5879947394533,10.4310163426224));
#46840=CARTESIAN_POINT('Ctrl Pts',(-22.4854565980335,26.5920208550813,10.4317848231876));
#46841=CARTESIAN_POINT('Ctrl Pts',(-22.4903941007061,26.5937447724024,10.4321165560944));
#46842=CARTESIAN_POINT('Ctrl Pts',(-22.4991216841054,26.5967681737169,10.4327031203373));
#46843=CARTESIAN_POINT('Ctrl Pts',(-22.5029100424305,26.5980726257605,10.4329577916154));
#46844=CARTESIAN_POINT('Ctrl Pts',(-22.5109660506878,26.6008297715119,10.4334994891419));
#46845=CARTESIAN_POINT('Ctrl Pts',(-22.5152343324541,26.6022805808135,10.4337865747312));
#46846=CARTESIAN_POINT('Ctrl Pts',(-22.5368410822363,26.6095742798648,10.4352402580337));
#46847=CARTESIAN_POINT('Ctrl Pts',(-22.5542257713685,26.6152783058002,10.436411216724));
#46848=CARTESIAN_POINT('Ctrl Pts',(-22.6258978182909,26.6381201973344,10.4412442716266));
#46849=CARTESIAN_POINT('Ctrl Pts',(-22.6805836184896,26.6539654267989,10.4449451334664));
#46850=CARTESIAN_POINT('Ctrl Pts',(-22.9574715594903,26.7263015817659,10.4637409459603));
#46851=CARTESIAN_POINT('Ctrl Pts',(-23.1848233839031,26.7604113079534,10.4794217523819));
#46852=CARTESIAN_POINT('Ctrl Pts',(-23.4933401491112,26.7734824375079,10.5001691331206));
#46853=CARTESIAN_POINT('Ctrl Pts',(-23.5729483528909,26.7739051974754,10.5054683205015));
#46854=CARTESIAN_POINT('Ctrl Pts',(-23.7091539135128,26.7695818683568,10.5143616640604));
#46855=CARTESIAN_POINT('Ctrl Pts',(-23.7657598625508,26.7662886911308,10.5180060663949));
#46856=CARTESIAN_POINT('Ctrl Pts',(-23.8319812801346,26.7606795724336,10.5221865443536));
#46857=CARTESIAN_POINT('Ctrl Pts',(-23.8417054408293,26.7598113922279,10.5227983121976));
#46858=CARTESIAN_POINT('Ctrl Pts',(-23.8543124063815,26.7586280648666,10.5235885783629));
#46859=CARTESIAN_POINT('Ctrl Pts',(-23.8571988046419,26.7583532088762,10.5237693169769));
#46860=CARTESIAN_POINT('Ctrl Pts',(-23.862163819886,26.7578736554042,10.5240798730951));
#46861=CARTESIAN_POINT('Ctrl Pts',(-23.8642426096241,26.7576708324453,10.5242097964911));
#46862=CARTESIAN_POINT('Ctrl Pts',(-23.8681884490219,26.7572819726916,10.524456213007));
#46863=CARTESIAN_POINT('Ctrl Pts',(-23.8700555195376,26.7570963276929,10.5245727271784));
#46864=CARTESIAN_POINT('Ctrl Pts',(-23.8743284972309,26.7566676917167,10.5248391909866));
#46865=CARTESIAN_POINT('Ctrl Pts',(-23.8767342904402,26.7564236236914,10.5249890786598));
#46866=CARTESIAN_POINT('Ctrl Pts',(-23.8841326964325,26.7556646408158,10.5254496015725));
#46867=CARTESIAN_POINT('Ctrl Pts',(-23.8891244133734,26.7551407672375,10.5257597308031));
#46868=CARTESIAN_POINT('Ctrl Pts',(-23.9265426620332,26.7511253763653,10.5280802195263));
#46869=CARTESIAN_POINT('Ctrl Pts',(-23.9589172322387,26.7471533108994,10.5300639254062));
#46870=CARTESIAN_POINT('Ctrl Pts',(-23.9997695085673,26.7415103416319,10.5325430043859));
#46871=CARTESIAN_POINT('Ctrl Pts',(-24.0083069195981,26.7402961212035,10.5330597542648));
#46872=CARTESIAN_POINT('Ctrl Pts',(-24.0202422753242,26.7385497309103,10.5337804350534));
#46873=CARTESIAN_POINT('Ctrl Pts',(-24.0236443184346,26.7380463779289,10.5339856594312));
#46874=CARTESIAN_POINT('Ctrl Pts',(-24.036553864194,26.7361152103764,10.5347636841201));
#46875=CARTESIAN_POINT('Ctrl Pts',(-24.0460558600688,26.7346502859263,10.5353348434018));
#46876=CARTESIAN_POINT('Ctrl Pts',(-24.0597309324058,26.7324793041945,10.5361548628734));
#46877=CARTESIAN_POINT('Ctrl Pts',(-24.0639093088402,26.7318075269824,10.5364051506095));
#46878=CARTESIAN_POINT('Ctrl Pts',(-24.0755404240493,26.7299140275347,10.5371011498845));
#46879=CARTESIAN_POINT('Ctrl Pts',(-24.082990250518,26.7286743291875,10.5375461277499));
#46880=CARTESIAN_POINT('Ctrl Pts',(-24.3552167058685,26.6823901190218,10.553778604314));
#46881=CARTESIAN_POINT('Ctrl Pts',(-24.6133561284165,26.6044456608113,10.5682945159859));
#46882=CARTESIAN_POINT('Ctrl Pts',(-24.9741050930122,26.4441542242742,10.5906675811731));
#46883=CARTESIAN_POINT('Ctrl Pts',(-25.086241183986,26.386228049148,10.597937183782));
#46884=CARTESIAN_POINT('Ctrl Pts',(-25.2407077058277,26.2945816238037,10.608616431837));
#46885=CARTESIAN_POINT('Ctrl Pts',(-25.2860378547698,26.2661372228601,10.6118364751075));
#46886=CARTESIAN_POINT('Ctrl Pts',(-25.3373605461971,26.2321226945501,10.6155905935662));
#46887=CARTESIAN_POINT('Ctrl Pts',(-25.3440673240266,26.2276413930406,10.6160833476486));
#46888=CARTESIAN_POINT('Ctrl Pts',(-25.3542007261504,26.2208153400088,10.6168311839908));
#46889=CARTESIAN_POINT('Ctrl Pts',(-25.3576397937218,26.2184890441195,10.6170855672015));
#46890=CARTESIAN_POINT('Ctrl Pts',(-25.3638194686595,26.2142914841526,10.6175437240084));
#46891=CARTESIAN_POINT('Ctrl Pts',(-25.3665617039221,26.2124226175113,10.6177474063336));
#46892=CARTESIAN_POINT('Ctrl Pts',(-25.3724409983222,26.2084024942934,10.6181849049041));
#46893=CARTESIAN_POINT('Ctrl Pts',(-25.3755771425727,26.2062499142798,10.6184187713607));
#46894=CARTESIAN_POINT('Ctrl Pts',(-25.3840287715977,26.2004268639372,10.6190503627662));
#46895=CARTESIAN_POINT('Ctrl Pts',(-25.3893370231811,26.1967459704757,10.6194484854597));
#46896=CARTESIAN_POINT('Ctrl Pts',(-25.4128051485247,26.1803677980986,10.6212150229026));
#46897=CARTESIAN_POINT('Ctrl Pts',(-25.4308445053855,26.1674996262599,10.6225899858126));
#46898=CARTESIAN_POINT('Ctrl Pts',(-25.4590045418694,26.1469705348221,10.6247638075597));
#46899=CARTESIAN_POINT('Ctrl Pts',(-25.4692153385196,26.1394339395328,10.6255578019092));
#46900=CARTESIAN_POINT('Ctrl Pts',(-25.48384435046,26.1285021866681,10.6267037509748));
#46901=CARTESIAN_POINT('Ctrl Pts',(-25.4882987847766,26.1251555056441,10.6270538136856));
#46902=CARTESIAN_POINT('Ctrl Pts',(-25.4942910263318,26.1206290897798,10.6275262572224));
#46903=CARTESIAN_POINT('Ctrl Pts',(-25.4958365000501,26.119459479575,10.6276482437869));
#46904=CARTESIAN_POINT('Ctrl Pts',(-25.5011850377363,26.1154041276422,10.6280708887614));
#46905=CARTESIAN_POINT('Ctrl Pts',(-25.5049827301577,26.1125113406648,10.628371820904));
#46906=CARTESIAN_POINT('Ctrl Pts',(-25.512193752647,26.1069931817093,10.6289448235678));
#46907=CARTESIAN_POINT('Ctrl Pts',(-25.5156082787859,26.1043693835626,10.6292168325383));
#46908=CARTESIAN_POINT('Ctrl Pts',(-25.7693656019002,25.9085664321569,10.6494827619479));
#46909=CARTESIAN_POINT('Ctrl Pts',(-25.9898799248703,25.6796275058191,10.6710531817898));
#46910=CARTESIAN_POINT('Ctrl Pts',(-26.2159666206192,25.3628290157788,10.6972403813263));
#46911=CARTESIAN_POINT('Ctrl Pts',(-26.2564101777454,25.3018737823719,10.7021247957741));
#46912=CARTESIAN_POINT('Ctrl Pts',(-26.330673999434,25.1812251084219,10.711431704681));
#46913=CARTESIAN_POINT('Ctrl Pts',(-26.3647334297483,25.1217212647439,10.7158616098211));
#46914=CARTESIAN_POINT('Ctrl Pts',(-26.4020327215134,25.0514482184307,10.720871905912));
#46915=CARTESIAN_POINT('Ctrl Pts',(-26.407143879593,25.0416983321162,10.721562209142));
#46916=CARTESIAN_POINT('Ctrl Pts',(-26.4137228852048,25.0289905058272,10.7224554743431));
#46917=CARTESIAN_POINT('Ctrl Pts',(-26.4152362053574,25.0260563843297,10.7226612751403));
#46918=CARTESIAN_POINT('Ctrl Pts',(-26.4176823371621,25.0212957259895,10.7229944612503));
#46919=CARTESIAN_POINT('Ctrl Pts',(-26.4186179136438,25.0194706245782,10.7231220219795));
#46920=CARTESIAN_POINT('Ctrl Pts',(-26.4204107340502,25.0159649915479,10.7233667045886));
#46921=CARTESIAN_POINT('Ctrl Pts',(-26.4212682420495,25.0142846052599,10.7234838428938));
#46922=CARTESIAN_POINT('Ctrl Pts',(-26.4232366796763,25.0104188434356,10.723752984353));
#46923=CARTESIAN_POINT('Ctrl Pts',(-26.4243465942659,25.0082329472304,10.7239049228347));
#46924=CARTESIAN_POINT('Ctrl Pts',(-26.427861087235,25.0012917998977,10.7243866132169));
#46925=CARTESIAN_POINT('Ctrl Pts',(-26.4302563826072,24.9965318188587,10.7247157799964));
#46926=CARTESIAN_POINT('Ctrl Pts',(-26.4505543853361,24.9559448160244,10.7275128223617));
#46927=CARTESIAN_POINT('Ctrl Pts',(-26.4678005921399,24.9197908905198,10.7299403045388));
#46928=CARTESIAN_POINT('Ctrl Pts',(-26.4874246138234,24.8765979924787,10.7327761600183));
#46929=CARTESIAN_POINT('Ctrl Pts',(-26.4904568500345,24.8698625838511,10.733216548521));
#46930=CARTESIAN_POINT('Ctrl Pts',(-26.4953538726103,24.8588843103488,10.7339314750054));
#46931=CARTESIAN_POINT('Ctrl Pts',(-26.4972326937314,24.8546477806102,10.7342066710095));
#46932=CARTESIAN_POINT('Ctrl Pts',(-26.5005965272106,24.8470183499256,10.7347010389309));
#46933=CARTESIAN_POINT('Ctrl Pts',(-26.5020848380141,24.8436269225083,10.7349203609288));
#46934=CARTESIAN_POINT('Ctrl Pts',(-26.5068051507016,24.8328201154468,10.7356178742657));
#46935=CARTESIAN_POINT('Ctrl Pts',(-26.5100151038521,24.8253950784762,10.7360950824805));
#46936=CARTESIAN_POINT('Ctrl Pts',(-26.5154403691719,24.8127148769824,10.7369067091626));
#46937=CARTESIAN_POINT('Ctrl Pts',(-26.517669735719,24.8074658082807,10.7372417187417));
#46938=CARTESIAN_POINT('Ctrl Pts',(-26.6423305341338,24.5117716309108,10.7560606869111));
#46939=CARTESIAN_POINT('Ctrl Pts',(-26.7215171657011,24.2049209831682,10.7728769383046));
#46940=CARTESIAN_POINT('Ctrl Pts',(-26.7669477794599,23.7781923874672,10.7975975107917));
#46941=CARTESIAN_POINT('Ctrl Pts',(-26.7729918350825,23.664410071898,10.8042939311957));
#46942=CARTESIAN_POINT('Ctrl Pts',(-26.7730042922185,23.5316397438179,10.8123301618297));
#46943=CARTESIAN_POINT('Ctrl Pts',(-26.7728395399343,23.5127252562369,10.8134801487195));
#46944=CARTESIAN_POINT('Ctrl Pts',(-26.7724019798592,23.4877437228323,10.8150061420369));
#46945=CARTESIAN_POINT('Ctrl Pts',(-26.7722785130801,23.4816741679591,10.8153774560738));
#46946=CARTESIAN_POINT('Ctrl Pts',(-26.7720604153553,23.4722607802433,10.8159542085373));
#46947=CARTESIAN_POINT('Ctrl Pts',(-26.7719777261741,23.4689166624007,10.8161592717701));
#46948=CARTESIAN_POINT('Ctrl Pts',(-26.7718018979418,23.4622272924601,10.8165698126992));
#46949=CARTESIAN_POINT('Ctrl Pts',(-26.7717087545637,23.4588820445849,10.8167752902833));
#46950=CARTESIAN_POINT('Ctrl Pts',(-26.7714894222586,23.4514223648541,10.8172338790897));
#46951=CARTESIAN_POINT('Ctrl Pts',(-26.7713605607507,23.4473080228201,10.8174870739362));
#46952=CARTESIAN_POINT('Ctrl Pts',(-26.7709615119465,23.4353022146965,10.8182266796868));
#46953=CARTESIAN_POINT('Ctrl Pts',(-26.7706702057895,23.4274115228575,10.8187137532332));
#46954=CARTESIAN_POINT('Ctrl Pts',(-26.7683558721294,23.3704058504887,10.8222397268425));
#46955=CARTESIAN_POINT('Ctrl Pts',(-26.7652384447557,23.3213440657745,10.8253128546951));
#46956=CARTESIAN_POINT('Ctrl Pts',(-26.7515547946116,23.1632358242845,10.8353482890459));
#46957=CARTESIAN_POINT('Ctrl Pts',(-26.7365517066242,23.0546606992704,10.8424460772234));
#46958=CARTESIAN_POINT('Ctrl Pts',(-26.6517514213579,22.6095874427737,10.8723660718261));
#46959=CARTESIAN_POINT('Ctrl Pts',(-26.5339142093063,22.2845969694627,10.8964658368068));
#46960=CARTESIAN_POINT('Ctrl Pts',(-26.366111136449,21.9827509351699,10.9182929659547));
#46961=CARTESIAN_POINT('Ctrl Pts',(-26.3652171858749,21.9811461194928,10.918408988645));
#46962=CARTESIAN_POINT('Ctrl Pts',(-26.3579201043826,21.9680727405011,10.9193539403912));
#46963=CARTESIAN_POINT('Ctrl Pts',(-26.3514481573238,21.9566424252233,10.9201788198388));
#46964=CARTESIAN_POINT('Ctrl Pts',(-26.3430933292041,21.9420948604869,10.9212266639652));
#46965=CARTESIAN_POINT('Ctrl Pts',(-26.3412749239718,21.9389410094193,10.9214537117862));
#46966=CARTESIAN_POINT('Ctrl Pts',(-26.3383751043843,21.9339311848979,10.9218141723359));
#46967=CARTESIAN_POINT('Ctrl Pts',(-26.3372971787775,21.9320732116921,10.9219478110332));
#46968=CARTESIAN_POINT('Ctrl Pts',(-26.3352788946983,21.9286023827981,10.9221973738033));
#46969=CARTESIAN_POINT('Ctrl Pts',(-26.3343389986212,21.9269892773994,10.9223133265918));
#46970=CARTESIAN_POINT('Ctrl Pts',(-26.3322257255409,21.92336958743,10.9225734401239));
#46971=CARTESIAN_POINT('Ctrl Pts',(-26.3310515815791,21.9213634593935,10.9227175496632));
#46972=CARTESIAN_POINT('Ctrl Pts',(-26.3275697259718,21.9154291403167,10.9231436900396));
#46973=CARTESIAN_POINT('Ctrl Pts',(-26.3252558415842,21.9115045494437,10.9234253187858));
#46974=CARTESIAN_POINT('Ctrl Pts',(-26.30694306519,21.8805941654071,10.9256420236892));
#46975=CARTESIAN_POINT('Ctrl Pts',(-26.2905585161613,21.8538371792182,10.9275522935291));
#46976=CARTESIAN_POINT('Ctrl Pts',(-26.2303257019679,21.7586237747518,10.9343347808559));
#46977=CARTESIAN_POINT('Ctrl Pts',(-26.1842788308701,21.6915881067284,10.939081791127));
#46978=CARTESIAN_POINT('Ctrl Pts',(-25.933327282883,21.3543380577292,10.9632052931394));
#46979=CARTESIAN_POINT('Ctrl Pts',(-25.6892621821821,21.1159666817246,10.9813393152816));
#46980=CARTESIAN_POINT('Ctrl Pts',(-25.3619883516068,20.8842514604203,11.0050733469101));
#46981=CARTESIAN_POINT('Ctrl Pts',(-25.3104570614142,20.8499511381906,11.0087869537192));
#46982=CARTESIAN_POINT('Ctrl Pts',(-25.2502143429537,20.8123096734548,11.0131145769786));
#46983=CARTESIAN_POINT('Ctrl Pts',(-25.2424354267687,20.8074951050111,11.013673121141));
#46984=CARTESIAN_POINT('Ctrl Pts',(-25.2309500962642,20.8004540022255,11.0144974441474));
#46985=CARTESIAN_POINT('Ctrl Pts',(-25.2272594841021,20.7982016714254,11.0147622730543));
#46986=CARTESIAN_POINT('Ctrl Pts',(-25.2206784524905,20.7942035103438,11.0152344215391));
#46987=CARTESIAN_POINT('Ctrl Pts',(-25.217789795141,20.7924547798942,11.0154416342804));
#46988=CARTESIAN_POINT('Ctrl Pts',(-25.2117523350789,20.7888127866905,11.0158746595001));
#46989=CARTESIAN_POINT('Ctrl Pts',(-25.208603034014,20.7869203632405,11.0161005023257));
#46990=CARTESIAN_POINT('Ctrl Pts',(-25.2005060204981,20.7820736731648,11.01668107053));
#46991=CARTESIAN_POINT('Ctrl Pts',(-25.1955536235319,20.7791272933432,11.0170360834278));
#46992=CARTESIAN_POINT('Ctrl Pts',(-25.17472592127,20.7668115714036,11.0185288004902));
#46993=CARTESIAN_POINT('Ctrl Pts',(-25.1587785284803,20.7575653906418,11.0196709754918));
#46994=CARTESIAN_POINT('Ctrl Pts',(-25.0501767987787,20.6958377310961,11.0274450676712));
#46995=CARTESIAN_POINT('Ctrl Pts',(-24.9550595855672,20.6478449917616,11.0342370429734));
#46996=CARTESIAN_POINT('Ctrl Pts',(-24.6216720757171,20.4998604764889,11.0580095661414));
#46997=CARTESIAN_POINT('Ctrl Pts',(-24.3738676499993,20.4238395764081,11.075713600696));
#46998=CARTESIAN_POINT('Ctrl Pts',(-24.0182666590555,20.3600016010271,11.099944426748));
#46999=CARTESIAN_POINT('Ctrl Pts',(-23.9160064393972,20.3466660557287,11.1067671732972));
#47000=CARTESIAN_POINT('Ctrl Pts',(-23.8068900658058,20.3377308165948,11.1137817078811));
#47001=CARTESIAN_POINT('Ctrl Pts',(-23.8005042582184,20.3372270620292,11.1141912508643));
#47002=CARTESIAN_POINT('Ctrl Pts',(-23.7680106938155,20.334761215262,11.1162701057945));
#47003=CARTESIAN_POINT('Ctrl Pts',(-23.7418802450931,20.3330982068341,11.1179252409949));
#47004=CARTESIAN_POINT('Ctrl Pts',(-23.7111052525198,20.3315159126458,11.1198527378459));
#47005=CARTESIAN_POINT('Ctrl Pts',(-23.7064785322951,20.3312880308064,11.1201419379402));
#47006=CARTESIAN_POINT('Ctrl Pts',(-23.699482134913,20.3309585542162,11.120578364503));
#47007=CARTESIAN_POINT('Ctrl Pts',(-23.6971128357321,20.3308495996138,11.1207260034949));
#47008=CARTESIAN_POINT('Ctrl Pts',(-23.6928741737281,20.3306593693827,11.1209898489777));
#47009=CARTESIAN_POINT('Ctrl Pts',(-23.6910048629802,20.3305771063009,11.1211061111608));
#47010=CARTESIAN_POINT('Ctrl Pts',(-23.6870214550233,20.330405283536,11.1213536518209));
#47011=CARTESIAN_POINT('Ctrl Pts',(-23.6849073466448,20.3303161781721,11.1214849040573));
#47012=CARTESIAN_POINT('Ctrl Pts',(-23.6792762860326,20.3300843959338,11.121834174255));
#47013=CARTESIAN_POINT('Ctrl Pts',(-23.6757591726004,20.3299453980314,11.1220519843567));
#47014=CARTESIAN_POINT('Ctrl Pts',(-23.6598828113058,20.3293440063675,11.1230336746236));
#47015=CARTESIAN_POINT('Ctrl Pts',(-23.6475209755071,20.3289469907293,11.1237939157647));
#47016=CARTESIAN_POINT('Ctrl Pts',(-23.3398233638043,20.3208377826917,11.1426209465618));
#47017=CARTESIAN_POINT('Ctrl Pts',(-23.044764394644,20.3536996662269,11.1585619801404));
#47018=CARTESIAN_POINT('Ctrl Pts',(-22.562375509171,20.4759948893336,11.1865701098311));
#47019=CARTESIAN_POINT('Ctrl Pts',(-22.3716127846577,20.5439673165184,11.198189196753));
#47020=CARTESIAN_POINT('Ctrl Pts',(-22.1770695567283,20.6346660176577,11.2112325393831));
#47021=CARTESIAN_POINT('Ctrl Pts',(-22.1656853732181,20.6400549473063,11.212000193099));
#47022=CARTESIAN_POINT('Ctrl Pts',(-22.1501699822298,20.6475111115298,11.2130525362298));
#47023=CARTESIAN_POINT('Ctrl Pts',(-22.1460110904959,20.6495207495204,11.2133352196204));
#47024=CARTESIAN_POINT('Ctrl Pts',(-22.1389386603159,20.6529570267536,11.2138169725945));
#47025=CARTESIAN_POINT('Ctrl Pts',(-22.1360229204009,20.6543791413472,11.2140158840542));
#47026=CARTESIAN_POINT('Ctrl Pts',(-22.1303863302755,20.6571388587126,11.2144009943718));
#47027=CARTESIAN_POINT('Ctrl Pts',(-22.1276652100543,20.6584759035752,11.2145871735325));
#47028=CARTESIAN_POINT('Ctrl Pts',(-22.1212108481018,20.6616586224197,11.2150294087414));
#47029=CARTESIAN_POINT('Ctrl Pts',(-22.117479296067,20.6635076934459,11.2152855836179));
#47030=CARTESIAN_POINT('Ctrl Pts',(-22.106622030793,20.668913959275,11.2160324074876));
#47031=CARTESIAN_POINT('Ctrl Pts',(-22.0995059448409,20.672490322798,11.2165237290734));
#47032=CARTESIAN_POINT('Ctrl Pts',(-22.0492942806905,20.6979589992145,11.2200036452253));
#47033=CARTESIAN_POINT('Ctrl Pts',(-22.0066847483304,20.7207910715358,11.2230252918054));
#47034=CARTESIAN_POINT('Ctrl Pts',(-21.8712287535633,20.7973447738146,11.232861540725));
#47035=CARTESIAN_POINT('Ctrl Pts',(-21.7805531745613,20.8547410774885,11.2398057705441));
#47036=CARTESIAN_POINT('Ctrl Pts',(-21.5112825753855,21.044635552459,11.2615442665771));
#47037=CARTESIAN_POINT('Ctrl Pts',(-21.3433958056176,21.1911672127142,11.2767580163808));
#47038=CARTESIAN_POINT('Ctrl Pts',(-21.123220882442,21.427565283442,11.298431053134));
#47039=CARTESIAN_POINT('Ctrl Pts',(-21.0579955317232,21.5045393291019,11.3051116739332));
#47040=CARTESIAN_POINT('Ctrl Pts',(-20.9749119951168,21.612473094337,11.3138584273169));
#47041=CARTESIAN_POINT('Ctrl Pts',(-20.9538036052451,21.6408491545473,11.316103349588));
#47042=CARTESIAN_POINT('Ctrl Pts',(-20.9304642500541,21.6733272938328,11.3186064207481));
#47043=CARTESIAN_POINT('Ctrl Pts',(-20.9277710722804,21.6770921048202,11.3188955787177));
#47044=CARTESIAN_POINT('Ctrl Pts',(-20.9237091294605,21.6827962529714,11.3193321707757));
#47045=CARTESIAN_POINT('Ctrl Pts',(-20.922334394684,21.6847313010402,11.3194800148158));
#47046=CARTESIAN_POINT('Ctrl Pts',(-20.9199481615072,21.6880979851151,11.3197367804938));
#47047=CARTESIAN_POINT('Ctrl Pts',(-20.9189356934341,21.6895289273153,11.3198457694407));
#47048=CARTESIAN_POINT('Ctrl Pts',(-20.9168193779014,21.6925251416988,11.320073675853));
#47049=CARTESIAN_POINT('Ctrl Pts',(-20.9157157590044,21.6940905709804,11.3201925770772));
#47050=CARTESIAN_POINT('Ctrl Pts',(-20.9130804753147,21.6978356767414,11.3204766236543));
#47051=CARTESIAN_POINT('Ctrl Pts',(-20.9115501118055,21.7000162768179,11.3206416786789));
#47052=CARTESIAN_POINT('Ctrl Pts',(-20.9064956385073,21.7072373722328,11.3211871726917));
#47053=CARTESIAN_POINT('Ctrl Pts',(-20.9029832259414,21.7122860976772,11.3215668100693));
#47054=CARTESIAN_POINT('Ctrl Pts',(-20.8572168639281,21.7784738163158,11.3265213354453));
#47055=CARTESIAN_POINT('Ctrl Pts',(-20.8170716272202,21.8410523870443,11.3309558503844));
#47056=CARTESIAN_POINT('Ctrl Pts',(-20.7428373173508,21.9660842622704,11.3394532427876));
#47057=CARTESIAN_POINT('Ctrl Pts',(-20.708581479622,22.0283865777841,11.3435215609221));
#47058=CARTESIAN_POINT('Ctrl Pts',(-20.5865759381276,22.268790780818,11.3587887783013));
#47059=CARTESIAN_POINT('Ctrl Pts',(-20.5132867138653,22.4537287950224,11.3696886034136));
#47060=CARTESIAN_POINT('Ctrl Pts',(-20.4365050382738,22.715830816055,11.3852170045572));
#47061=CARTESIAN_POINT('Ctrl Pts',(-20.4180253173361,22.7881273754,11.389504704196));
#47062=CARTESIAN_POINT('Ctrl Pts',(-20.3960161591698,22.8886544166408,11.3955162303357));
#47063=CARTESIAN_POINT('Ctrl Pts',(-20.3903257736931,22.9163897894362,11.3971798505208));
#47064=CARTESIAN_POINT('Ctrl Pts',(-20.3829315106859,22.9550077974361,11.3995051305546));
#47065=CARTESIAN_POINT('Ctrl Pts',(-20.3809167770313,22.9658300699515,11.4001577289162));
#47066=CARTESIAN_POINT('Ctrl Pts',(-20.3694607810698,23.0291685723939,11.4039831900359));
#47067=CARTESIAN_POINT('Ctrl Pts',(-20.3612699311525,23.0818999783438,11.407192541446));
#47068=CARTESIAN_POINT('Ctrl Pts',(-20.3532637072807,23.1434889050007,11.4109773372298));
#47069=CARTESIAN_POINT('Ctrl Pts',(-20.352170638663,23.1521741543488,11.4115119002514));
#47070=CARTESIAN_POINT('Ctrl Pts',(-20.3505943388137,23.1651247131689,11.4123102612106));
#47071=CARTESIAN_POINT('Ctrl Pts',(-20.3500842156329,23.1693867594534,11.4125732084622));
#47072=CARTESIAN_POINT('Ctrl Pts',(-20.3491895922107,23.1769899816446,11.4130426610465));
#47073=CARTESIAN_POINT('Ctrl Pts',(-20.348801803629,23.1803307704538,11.4132490621287));
#47074=CARTESIAN_POINT('Ctrl Pts',(-20.3479952982837,23.1873750526616,11.413684544795));
#47075=CARTESIAN_POINT('Ctrl Pts',(-20.3475777754212,23.1910786753729,11.4139136637805));
#47076=CARTESIAN_POINT('Ctrl Pts',(-20.3465054919453,23.2007408706978,11.4145118178363));
#47077=CARTESIAN_POINT('Ctrl Pts',(-20.3458609319735,23.206700540382,11.4148811745026));
#47078=CARTESIAN_POINT('Ctrl Pts',(-20.3430901333203,23.2330059648974,11.4165133322204));
#47079=CARTESIAN_POINT('Ctrl Pts',(-20.3411410514901,23.2533695408764,11.4177817100035));
#47080=CARTESIAN_POINT('Ctrl Pts',(-20.3365640804233,23.3065192858193,11.4211055253391));
#47081=CARTESIAN_POINT('Ctrl Pts',(-20.3342440660622,23.3393289039834,11.4231705260076));
#47082=CARTESIAN_POINT('Ctrl Pts',(-20.3261923031749,23.4848164055113,11.4323883093344));
#47083=CARTESIAN_POINT('Ctrl Pts',(-20.3258781914935,23.5977031345775,11.4397063093796));
#47084=CARTESIAN_POINT('Ctrl Pts',(-20.3402581377045,23.8867875778558,11.4588454321717));
#47085=CARTESIAN_POINT('Ctrl Pts',(-20.3635237126299,24.0621813067796,11.4708531778101));
#47086=CARTESIAN_POINT('Ctrl Pts',(-20.4261041984751,24.350091362431,11.4907547148228));
#47087=CARTESIAN_POINT('Ctrl Pts',(-20.4574882496792,24.4639583600217,11.4986707084414));
#47088=CARTESIAN_POINT('Ctrl Pts',(-20.4960111090153,24.5787154634658,11.5065434744349));
#47089=CARTESIAN_POINT('Ctrl Pts',(-20.4969755317072,24.5815750959363,11.5067395855296));
#47090=CARTESIAN_POINT('Ctrl Pts',(-20.5148614195832,24.6343639759012,11.5103584485964));
#47091=CARTESIAN_POINT('Ctrl Pts',(-20.5330027549045,24.6838756695719,11.5137303842427));
#47092=CARTESIAN_POINT('Ctrl Pts',(-20.5544602875104,24.7382674288478,11.5173925380823));
#47093=CARTESIAN_POINT('Ctrl Pts',(-20.5565828246385,24.743605896143,11.5177515165796));
#47094=CARTESIAN_POINT('Ctrl Pts',(-20.5595753913272,24.7510743744164,11.5182530562658));
#47095=CARTESIAN_POINT('Ctrl Pts',(-20.560433427811,24.7532091319125,11.5183963375356));
#47096=CARTESIAN_POINT('Ctrl Pts',(-20.5620072922888,24.7571127526465,11.5186581991264));
#47097=CARTESIAN_POINT('Ctrl Pts',(-20.5627224062121,24.7588819013278,11.5187768229576));
#47098=CARTESIAN_POINT('Ctrl Pts',(-20.5641778123513,24.7624733043297,11.5190175208003));
#47099=CARTESIAN_POINT('Ctrl Pts',(-20.5649182017018,24.7642955166523,11.51913958868));
#47100=CARTESIAN_POINT('Ctrl Pts',(-20.5667616070543,24.7688205383609,11.5194425736629));
#47101=CARTESIAN_POINT('Ctrl Pts',(-20.567866630913,24.7715225359368,11.5196233681407));
#47102=CARTESIAN_POINT('Ctrl Pts',(-20.571927881771,24.7814146979628,11.520284821565));
#47103=CARTESIAN_POINT('Ctrl Pts',(-20.5749064825798,24.7885957357251,11.5207641295584));
#47104=CARTESIAN_POINT('Ctrl Pts',(-20.6532720103714,24.9756102566819,11.5332259062039));
#47105=CARTESIAN_POINT('Ctrl Pts',(-20.7448136597775,25.1482760674421,11.5442416706843));
#47106=CARTESIAN_POINT('Ctrl Pts',(-20.9218719331134,25.4195700115963,11.5623837291471));
#47107=CARTESIAN_POINT('Ctrl Pts',(-20.998732905295,25.5231892641634,11.5695433776873));
#47108=CARTESIAN_POINT('Ctrl Pts',(-21.1975683583782,25.7601270344267,11.5870433995674));
#47109=CARTESIAN_POINT('Ctrl Pts',(-21.3249280914906,25.8883253830876,11.5974939427606));
#47110=CARTESIAN_POINT('Ctrl Pts',(-21.4712720927064,26.0127909935341,11.6091748308002));
#47111=CARTESIAN_POINT('Ctrl Pts',(-21.4802548692204,26.0203466621702,11.6098904997992));
#47112=CARTESIAN_POINT('Ctrl Pts',(-21.4927247472399,26.0307196393112,11.6108822580019));
#47113=CARTESIAN_POINT('Ctrl Pts',(-21.4961768271812,26.0335790618892,11.6111566278147));
#47114=CARTESIAN_POINT('Ctrl Pts',(-21.5021089114825,26.0384718867002,11.6116278006898));
#47115=CARTESIAN_POINT('Ctrl Pts',(-21.5045860130364,26.040508812074,11.6118244602784));
#47116=CARTESIAN_POINT('Ctrl Pts',(-21.5094211609765,26.0444726808201,11.6122081517916));
#47117=CARTESIAN_POINT('Ctrl Pts',(-21.5117789065443,26.0463999863699,11.6123951686996));
#47118=CARTESIAN_POINT('Ctrl Pts',(-21.5174409920382,26.0510150052697,11.6128440942085));
#47119=CARTESIAN_POINT('Ctrl Pts',(-21.5207479289139,26.0536995097655,11.6131061320981));
#47120=CARTESIAN_POINT('Ctrl Pts',(-21.5306060667776,26.0616697763789,11.6138868209155));
#47121=CARTESIAN_POINT('Ctrl Pts',(-21.5371726278454,26.0669364051107,11.6144062412082));
#47122=CARTESIAN_POINT('Ctrl Pts',(-21.5948479100937,26.1128239931345,11.6189633055014));
#47123=CARTESIAN_POINT('Ctrl Pts',(-21.6471561227556,26.1519063863036,11.6230618724274));
#47124=CARTESIAN_POINT('Ctrl Pts',(-21.7846427491397,26.2482646213656,11.6337598546252));
#47125=CARTESIAN_POINT('Ctrl Pts',(-21.8714303682177,26.3031055551097,11.6404444481765));
#47126=CARTESIAN_POINT('Ctrl Pts',(-21.9983872080542,26.3750906952972,11.6501127898601));
#47127=CARTESIAN_POINT('Ctrl Pts',(-22.036514291001,26.395703530941,11.6530024603944));
#47128=CARTESIAN_POINT('Ctrl Pts',(-22.0750360887345,26.4155368123409,11.6559056162233));
#47129=CARTESIAN_POINT('Origin',(-23.5502525316942,23.5502525316942,-77.3107734492734));
#47130=CARTESIAN_POINT('',(-22.0759547750155,26.4137025163195,13.1538544762661));
#47131=CARTESIAN_POINT('',(-22.0750360153462,26.4155367745564,12.9101997884793));
#47132=CARTESIAN_POINT('',(-22.0750360153461,26.4155367745563,-77.3107734492734));
#47133=CARTESIAN_POINT('',(-26.7732842589511,23.5513999092453,12.3107735328638));
#47134=CARTESIAN_POINT('Ctrl Pts',(-26.777835819343,23.5513797621693,12.3107748823706));
#47135=CARTESIAN_POINT('Ctrl Pts',(-26.7732053868241,22.5449087652806,12.3731671879169));
#47136=CARTESIAN_POINT('Ctrl Pts',(-25.7246919797972,20.4607039664501,12.5018551305882));
#47137=CARTESIAN_POINT('Ctrl Pts',(-22.1726033898576,19.9960316527802,12.6968387103845));
#47138=CARTESIAN_POINT('Ctrl Pts',(-19.8153491088126,22.7880848100881,12.8957256217594));
#47139=CARTESIAN_POINT('Ctrl Pts',(-20.6386024886415,25.4631247734142,13.0480642103866));
#47140=CARTESIAN_POINT('Ctrl Pts',(-21.7898377407983,26.26967571401,13.1341071618889));
#47141=CARTESIAN_POINT('Ctrl Pts',(-22.075954775016,26.4137025163198,13.1538544762662));
#47142=CARTESIAN_POINT('Ctrl Pts',(-22.075036015346,26.4155367745563,11.9036974267448));
#47143=CARTESIAN_POINT('Ctrl Pts',(-22.1633969361913,26.4610301632682,11.9098683281394));
#47144=CARTESIAN_POINT('Ctrl Pts',(-22.2540160014955,26.5025104832484,11.9160392295341));
#47145=CARTESIAN_POINT('Ctrl Pts',(-22.3464929848755,26.5397475586081,11.9222101309288));
#47146=CARTESIAN_POINT('Ctrl Pts',(-22.4388482208512,26.5769356107719,11.9283729082346));
#47147=CARTESIAN_POINT('Ctrl Pts',(-22.5330561135148,26.6098913611028,11.9345356855405));
#47148=CARTESIAN_POINT('Ctrl Pts',(-22.6286922229561,26.6384306612487,11.9406984628463));
#47149=CARTESIAN_POINT('Ctrl Pts',(-22.724230684154,26.6669408216423,11.9468549477133));
#47150=CARTESIAN_POINT('Ctrl Pts',(-22.8211940487476,26.6910433736225,11.9530114325802));
#47151=CARTESIAN_POINT('Ctrl Pts',(-22.9191391990101,26.7106027533957,11.9591679174471));
#47152=CARTESIAN_POINT('Ctrl Pts',(-23.0170178062356,26.7301488447055,11.9653202196547));
#47153=CARTESIAN_POINT('Ctrl Pts',(-23.115876448277,26.7451578151042,11.9714725218622));
#47154=CARTESIAN_POINT('Ctrl Pts',(-23.2152590673981,26.755544552927,11.9776248240697));
#47155=CARTESIAN_POINT('Ctrl Pts',(-23.3146074535599,26.7659277129736,11.9837750070787));
#47156=CARTESIAN_POINT('Ctrl Pts',(-23.414479026507,26.7716917590445,11.9899251900876));
#47157=CARTESIAN_POINT('Ctrl Pts',(-23.5144107150789,26.7728032181353,11.9960753730965));
#47158=CARTESIAN_POINT('Ctrl Pts',(-23.6143347162029,26.7739145917248,12.0022250829901));
#47159=CARTESIAN_POINT('Ctrl Pts',(-23.7143183893491,26.7703740852893,12.0083747928837));
#47160=CARTESIAN_POINT('Ctrl Pts',(-23.8138977699165,26.7622003442937,12.0145245027773));
#47161=CARTESIAN_POINT('Ctrl Pts',(-23.9134961303172,26.7540250453827,12.0206753848058));
#47162=CARTESIAN_POINT('Ctrl Pts',(-24.0126896121068,26.741214793225,12.0268262668344));
#47163=CARTESIAN_POINT('Ctrl Pts',(-24.1110194905167,26.7238400884496,12.0329771488629));
#47164=CARTESIAN_POINT('Ctrl Pts',(-24.2094564287027,26.706446466413,12.0391347278595));
#47165=CARTESIAN_POINT('Ctrl Pts',(-24.3070274576873,26.6844785452428,12.045292306856));
#47166=CARTESIAN_POINT('Ctrl Pts',(-24.4032843061283,26.6580579236558,12.0514498858525));
#47167=CARTESIAN_POINT('Ctrl Pts',(-24.4995978549259,26.6316217389303,12.0576110919876));
#47168=CARTESIAN_POINT('Ctrl Pts',(-24.5945952688175,26.6007277653805,12.0637722981227));
#47169=CARTESIAN_POINT('Ctrl Pts',(-24.6878456816555,26.5655467773129,12.0699335042578));
#47170=CARTESIAN_POINT('Ctrl Pts',(-24.7812484867023,26.5303082955751,12.0761047791935));
#47171=CARTESIAN_POINT('Ctrl Pts',(-24.8728981906794,26.4907689806387,12.0822760541292));
#47172=CARTESIAN_POINT('Ctrl Pts',(-24.9623860181702,26.4471468305724,12.0884473290649));
#47173=CARTESIAN_POINT('Ctrl Pts',(-25.0190868967554,26.4195071581847,12.0923575447965));
#47174=CARTESIAN_POINT('Ctrl Pts',(-25.0749203560244,26.3902292782621,12.0962677605281));
#47175=CARTESIAN_POINT('Ctrl Pts',(-25.1297884600919,26.3593776291935,12.1001779762598));
#47176=CARTESIAN_POINT('Ctrl Pts',(-25.2163951773887,26.3106797546373,12.1063500675721));
#47177=CARTESIAN_POINT('Ctrl Pts',(-25.3009002478314,26.2578871680822,12.1125221588844));
#47178=CARTESIAN_POINT('Ctrl Pts',(-25.3828907486128,26.2012060824735,12.1186942501967));
#47179=CARTESIAN_POINT('Ctrl Pts',(-25.4647701603715,26.1446017941322,12.1248579789355));
#47180=CARTESIAN_POINT('Ctrl Pts',(-25.5441414200523,26.084119723353,12.1310217076743));
#47181=CARTESIAN_POINT('Ctrl Pts',(-25.6206165445705,26.0200117136159,12.1371854364131));
#47182=CARTESIAN_POINT('Ctrl Pts',(-25.6970106508718,25.9559716202984,12.1433426352598));
#47183=CARTESIAN_POINT('Ctrl Pts',(-25.7705143907708,25.888313502488,12.1494998341065));
#47184=CARTESIAN_POINT('Ctrl Pts',(-25.8407699146686,25.8173316394433,12.1556570329531));
#47185=CARTESIAN_POINT('Ctrl Pts',(-25.9109740860388,25.746401659836,12.1618097312609));
#47186=CARTESIAN_POINT('Ctrl Pts',(-25.9779344571518,25.6721530729742,12.1679624295686));
#47187=CARTESIAN_POINT('Ctrl Pts',(-26.041328055983,25.5949188357128,12.1741151278763));
#47188=CARTESIAN_POINT('Ctrl Pts',(-26.1046976158714,25.517713885784,12.180265493072));
#47189=CARTESIAN_POINT('Ctrl Pts',(-26.1645028156326,25.4375258704559,12.1864158582678));
#47190=CARTESIAN_POINT('Ctrl Pts',(-26.2204598120355,25.3547221608408,12.1925662234635));
#47191=CARTESIAN_POINT('Ctrl Pts',(-26.276410559609,25.271927698081,12.1987159018358));
#47192=CARTESIAN_POINT('Ctrl Pts',(-26.32851371497,25.1865184816921,12.204865580208));
#47193=CARTESIAN_POINT('Ctrl Pts',(-26.3765283518551,25.0988914666541,12.2110152585802));
#47194=CARTESIAN_POINT('Ctrl Pts',(-26.4245504720781,25.0112507944774,12.2171658954127));
#47195=CARTESIAN_POINT('Ctrl Pts',(-26.4684825993837,24.9213920180873,12.2233165322451));
#47196=CARTESIAN_POINT('Ctrl Pts',(-26.508129901316,24.8297364232611,12.2294671690776));
#47197=CARTESIAN_POINT('Ctrl Pts',(-26.5478196175327,24.7379827762025,12.2356243857994));
#47198=CARTESIAN_POINT('Ctrl Pts',(-26.5832151820521,24.6444288717054,12.2417816025212));
#47199=CARTESIAN_POINT('Ctrl Pts',(-26.6141701071009,24.5495155869575,12.247938819243));
#47200=CARTESIAN_POINT('Ctrl Pts',(-26.6451423017755,24.4545493504767,12.2540994710509));
#47201=CARTESIAN_POINT('Ctrl Pts',(-26.6716688079092,24.3582226422454,12.2602601228587));
#47202=CARTESIAN_POINT('Ctrl Pts',(-26.6936537386872,24.2609890612009,12.2664207746665));
#47203=CARTESIAN_POINT('Ctrl Pts',(-26.7156754580723,24.1635927737985,12.2725917354355));
#47204=CARTESIAN_POINT('Ctrl Pts',(-26.7331403459201,24.0652870102811,12.2787626962046));
#47205=CARTESIAN_POINT('Ctrl Pts',(-26.7460040806895,23.9665332057521,12.2849336569736));
#47206=CARTESIAN_POINT('Ctrl Pts',(-26.7558232109672,23.8911525725633,12.289644067194));
#47207=CARTESIAN_POINT('Ctrl Pts',(-26.7629625202242,23.8155110489789,12.2943544774143));
#47208=CARTESIAN_POINT('Ctrl Pts',(-26.7674227389952,23.7398136557539,12.2990648876347));
#47209=CARTESIAN_POINT('Ctrl Pts',(-26.7711182944392,23.6770938816813,12.3029677415141));
#47210=CARTESIAN_POINT('Ctrl Pts',(-26.772979921602,23.6142649885854,12.3068705953935));
#47211=CARTESIAN_POINT('Ctrl Pts',(-26.7730023270025,23.551401157192,12.3107734492729));
#47212=CARTESIAN_POINT('',(-26.7730010877972,23.5472596439823,12.0640407997644));
#47213=CARTESIAN_POINT('Ctrl Pts',(-22.0750360887345,26.4155368123409,11.6559056162233));
#47214=CARTESIAN_POINT('Ctrl Pts',(-22.1583819015529,26.4584481263603,11.6621868880363));
#47215=CARTESIAN_POINT('Ctrl Pts',(-22.2435753494475,26.4977101766977,11.6685327647814));
#47216=CARTESIAN_POINT('Ctrl Pts',(-22.4944958418206,26.6003239394625,11.6868829776968));
#47217=CARTESIAN_POINT('Ctrl Pts',(-22.6638924415869,26.653788603226,11.6988702860808));
#47218=CARTESIAN_POINT('Ctrl Pts',(-22.8411604157104,26.6940282146079,11.7105090997077));
#47219=CARTESIAN_POINT('Ctrl Pts',(-22.8454810142825,26.6949996252062,11.710792225488));
#47220=CARTESIAN_POINT('Ctrl Pts',(-22.8548833172774,26.6970932173249,11.711407135838));
#47221=CARTESIAN_POINT('Ctrl Pts',(-22.8599657777958,26.6982120046405,11.7117387569925));
#47222=CARTESIAN_POINT('Ctrl Pts',(-22.8732665170419,26.7011060968989,11.7126045491575));
#47223=CARTESIAN_POINT('Ctrl Pts',(-22.8814891356707,26.7028615745325,11.7131377374304));
#47224=CARTESIAN_POINT('Ctrl Pts',(-22.8930838902174,26.7052895775527,11.7138866114003));
#47225=CARTESIAN_POINT('Ctrl Pts',(-22.8964502929972,26.7059888985347,11.714103685199));
#47226=CARTESIAN_POINT('Ctrl Pts',(-22.9116191278717,26.7091146880194,11.7150801986262));
#47227=CARTESIAN_POINT('Ctrl Pts',(-22.9234341987885,26.711480384223,11.715836421878));
#47228=CARTESIAN_POINT('Ctrl Pts',(-22.9387604333931,26.714459805925,11.7168114516609));
#47229=CARTESIAN_POINT('Ctrl Pts',(-22.9422595321867,26.7151340102685,11.7170336590572));
#47230=CARTESIAN_POINT('Ctrl Pts',(-22.947625038379,26.7161586062532,11.7173737713073));
#47231=CARTESIAN_POINT('Ctrl Pts',(-22.9494906346947,26.716513151382,11.7174919141692));
#47232=CARTESIAN_POINT('Ctrl Pts',(-22.9531706313834,26.7172091426108,11.7177247299621));
#47233=CARTESIAN_POINT('Ctrl Pts',(-22.954985002299,26.7175506767369,11.7178394071403));
#47234=CARTESIAN_POINT('Ctrl Pts',(-22.9590278497894,26.7183080989157,11.7180946918475));
#47235=CARTESIAN_POINT('Ctrl Pts',(-22.9612564668359,26.7187231938835,11.7182352531147));
#47236=CARTESIAN_POINT('Ctrl Pts',(-22.9658594701741,26.7195755100242,11.7185252337981));
#47237=CARTESIAN_POINT('Ctrl Pts',(-22.9682339145395,26.720012415455,11.7186746350598));
#47238=CARTESIAN_POINT('Ctrl Pts',(-22.980835024686,26.7223164238251,11.7194665362847));
#47239=CARTESIAN_POINT('Ctrl Pts',(-22.9910703451991,26.7241367328508,11.7201063836719));
#47240=CARTESIAN_POINT('Ctrl Pts',(-23.097719087717,26.7425718448006,11.7267399263721));
#47241=CARTESIAN_POINT('Ctrl Pts',(-23.1948435507788,26.7548395265761,11.7324970744747));
#47242=CARTESIAN_POINT('Ctrl Pts',(-23.453293512803,26.7755857935668,11.7474218260412));
#47243=CARTESIAN_POINT('Ctrl Pts',(-23.6149530678943,26.7763950254761,11.7563617826249));
#47244=CARTESIAN_POINT('Ctrl Pts',(-24.0131954265344,26.7484302245771,11.7787016166142));
#47245=CARTESIAN_POINT('Ctrl Pts',(-24.2477784870213,26.7055797608932,11.7921904611814));
#47246=CARTESIAN_POINT('Ctrl Pts',(-24.4860359704883,26.63417015758,11.807284655181));
#47247=CARTESIAN_POINT('Ctrl Pts',(-24.4965567610809,26.6309581113191,11.8079539458553));
#47248=CARTESIAN_POINT('Ctrl Pts',(-24.5134210731075,26.6257148200039,11.8090313248342));
#47249=CARTESIAN_POINT('Ctrl Pts',(-24.51977516248,26.6237176434739,11.809438294802));
#47250=CARTESIAN_POINT('Ctrl Pts',(-24.5301704416099,26.6204148218703,11.8101058153326));
#47251=CARTESIAN_POINT('Ctrl Pts',(-24.5342153443628,26.6191208542529,11.8103659809809));
#47252=CARTESIAN_POINT('Ctrl Pts',(-24.5414540350917,26.6167894088267,11.8108323387636));
#47253=CARTESIAN_POINT('Ctrl Pts',(-24.5446487871529,26.6157549254537,11.8110384318356));
#47254=CARTESIAN_POINT('Ctrl Pts',(-24.5514107768075,26.6135536623918,11.8114752192641));
#47255=CARTESIAN_POINT('Ctrl Pts',(-24.5549776023186,26.6123856413679,11.8117059543817));
#47256=CARTESIAN_POINT('Ctrl Pts',(-24.5622262301198,26.6099979197232,11.812175552864));
#47257=CARTESIAN_POINT('Ctrl Pts',(-24.5659078863463,26.6087777982608,11.8124144298487));
#47258=CARTESIAN_POINT('Ctrl Pts',(-24.5750467197972,26.6057308171349,11.8130082910244));
#47259=CARTESIAN_POINT('Ctrl Pts',(-24.5805012074329,26.6038959860318,11.8133635390273));
#47260=CARTESIAN_POINT('Ctrl Pts',(-24.6383269017339,26.5842714745622,11.8171382881326));
#47261=CARTESIAN_POINT('Ctrl Pts',(-24.6902339669244,26.565151948513,11.8206017839665));
#47262=CARTESIAN_POINT('Ctrl Pts',(-24.8654369191102,26.4954460164466,11.83256101336));
#47263=CARTESIAN_POINT('Ctrl Pts',(-24.986063359095,26.438559000576,11.8412641988081));
#47264=CARTESIAN_POINT('Ctrl Pts',(-25.1832705150222,26.3301446170131,11.8562583103202));
#47265=CARTESIAN_POINT('Ctrl Pts',(-25.2617996061271,26.2824957697177,11.8624493163574));
#47266=CARTESIAN_POINT('Ctrl Pts',(-25.52348486242,26.10800061983,11.8837283106694));
#47267=CARTESIAN_POINT('Ctrl Pts',(-25.6954977158155,25.965550801648,11.8988979644344));
#47268=CARTESIAN_POINT('Ctrl Pts',(-25.8606563609484,25.7971001946111,11.9137873562586));
#47269=CARTESIAN_POINT('Ctrl Pts',(-25.8697997123429,25.7876597734501,11.9146126792152));
#47270=CARTESIAN_POINT('Ctrl Pts',(-25.8814024553184,25.7755324814229,11.915661008562));
#47271=CARTESIAN_POINT('Ctrl Pts',(-25.8839152207294,25.7728971895725,11.9158881026453));
#47272=CARTESIAN_POINT('Ctrl Pts',(-25.8879033149234,25.7687004109248,11.9162486201375));
#47273=CARTESIAN_POINT('Ctrl Pts',(-25.8893815485406,25.7671417079516,11.9163822696364));
#47274=CARTESIAN_POINT('Ctrl Pts',(-25.8921415706526,25.7642256067751,11.9166318421381));
#47275=CARTESIAN_POINT('Ctrl Pts',(-25.8934237295114,25.7628685819216,11.9167477938787));
#47276=CARTESIAN_POINT('Ctrl Pts',(-25.8962994620486,25.7598196307186,11.9170078916945));
#47277=CARTESIAN_POINT('Ctrl Pts',(-25.8978923816025,25.7581270978144,11.9171519865928));
#47278=CARTESIAN_POINT('Ctrl Pts',(-25.9011907888867,25.7546148189507,11.9174504088359));
#47279=CARTESIAN_POINT('Ctrl Pts',(-25.9028959988638,25.7527948125811,11.9176047146762));
#47280=CARTESIAN_POINT('Ctrl Pts',(-25.9073338930857,25.7480471210699,11.9180063810837));
#47281=CARTESIAN_POINT('Ctrl Pts',(-25.9100632463183,25.7451163071618,11.9182534873194));
#47282=CARTESIAN_POINT('Ctrl Pts',(-25.9442779216337,25.7082385630836,11.9213522518531));
#47283=CARTESIAN_POINT('Ctrl Pts',(-25.9750356074631,25.6736198715369,11.9241495062405));
#47284=CARTESIAN_POINT('Ctrl Pts',(-26.0799581081083,25.5502719416452,11.9337830736277));
#47285=CARTESIAN_POINT('Ctrl Pts',(-26.1500904763527,25.4582188643049,11.9403909800539));
#47286=CARTESIAN_POINT('Ctrl Pts',(-26.2403333792828,25.3255247721238,11.9494380567717));
#47287=CARTESIAN_POINT('Ctrl Pts',(-26.2647632193281,25.2879401675862,11.9519505237983));
#47288=CARTESIAN_POINT('Ctrl Pts',(-26.3130386008662,25.2101661195729,11.9570717531765));
#47289=CARTESIAN_POINT('Ctrl Pts',(-26.3368098353016,25.1699433630333,11.9596794795737));
#47290=CARTESIAN_POINT('Ctrl Pts',(-26.4810979108476,24.913212282793,11.9761439799149));
#47291=CARTESIAN_POINT('Ctrl Pts',(-26.5771627767355,24.6839646348247,11.9901384764632));
#47292=CARTESIAN_POINT('Ctrl Pts',(-26.6504932628538,24.4305276022776,12.0061348066016));
#47293=CARTESIAN_POINT('Ctrl Pts',(-26.6548522781249,24.4150283354731,12.0071147061851));
#47294=CARTESIAN_POINT('Ctrl Pts',(-26.6605933062523,24.3940120716357,12.0084458061184));
#47295=CARTESIAN_POINT('Ctrl Pts',(-26.6620771752929,24.3885229426941,12.0087936900645));
#47296=CARTESIAN_POINT('Ctrl Pts',(-26.6643909449012,24.3798730383238,12.0093422514946));
#47297=CARTESIAN_POINT('Ctrl Pts',(-26.6652305831348,24.3767148602656,12.009542612382));
#47298=CARTESIAN_POINT('Ctrl Pts',(-26.6668382690031,24.370630527986,12.0099287604746));
#47299=CARTESIAN_POINT('Ctrl Pts',(-26.6676070031501,24.3677045571932,12.0101145251773));
#47300=CARTESIAN_POINT('Ctrl Pts',(-26.6694107353925,24.360799610099,12.0105530636269));
#47301=CARTESIAN_POINT('Ctrl Pts',(-26.6704422396957,24.356819734004,12.0108059503631));
#47302=CARTESIAN_POINT('Ctrl Pts',(-26.6725567560446,24.3485964877967,12.0113287223218));
#47303=CARTESIAN_POINT('Ctrl Pts',(-26.6736387395095,24.3443528642511,12.0115986403203));
#47304=CARTESIAN_POINT('Ctrl Pts',(-26.6764139638471,24.3333747970601,12.012297275495));
#47305=CARTESIAN_POINT('Ctrl Pts',(-26.6780940879305,24.3266370886384,12.0127264165809));
#47306=CARTESIAN_POINT('Ctrl Pts',(-26.6913132929716,24.2728854394685,12.0161529211494));
#47307=CARTESIAN_POINT('Ctrl Pts',(-26.7018129830375,24.225624529109,12.019183659344));
#47308=CARTESIAN_POINT('Ctrl Pts',(-26.7525202735369,23.970350280686,12.035661289225));
#47309=CARTESIAN_POINT('Ctrl Pts',(-26.7731978449979,23.7590327634544,12.0497328038615));
#47310=CARTESIAN_POINT('Ctrl Pts',(-26.7730011414961,23.5472591188997,12.0640407412713));
#47311=CARTESIAN_POINT('Ctrl Pts',(-26.7730011419778,23.5472596376123,12.0640407062258));
#47312=CARTESIAN_POINT('Ctrl Pts',(-26.7727976210084,23.328108239907,12.078847102146));
#47313=CARTESIAN_POINT('Ctrl Pts',(-26.7502410738742,23.109526304479,12.0938263018387));
#47314=CARTESIAN_POINT('Ctrl Pts',(-26.6994140844638,22.8648004766997,12.1098371960409));
#47315=CARTESIAN_POINT('Ctrl Pts',(-26.6927306461825,22.8347845201557,12.1117867810493));
#47316=CARTESIAN_POINT('Ctrl Pts',(-26.6847124201125,22.8010568884623,12.1139578945829));
#47317=CARTESIAN_POINT('Ctrl Pts',(-26.6837995539451,22.7972479077596,12.1142028036925));
#47318=CARTESIAN_POINT('Ctrl Pts',(-26.6823027138725,22.7910521256905,12.1146007084122));
#47319=CARTESIAN_POINT('Ctrl Pts',(-26.6817229537988,22.7886643255492,12.114753943577));
#47320=CARTESIAN_POINT('Ctrl Pts',(-26.6805957685026,22.7840449476642,12.1150501649778));
#47321=CARTESIAN_POINT('Ctrl Pts',(-26.6800486867298,22.7818132887731,12.115193170924));
#47322=CARTESIAN_POINT('Ctrl Pts',(-26.6790531842497,22.7777711286668,12.1154520093233));
#47323=CARTESIAN_POINT('Ctrl Pts',(-26.6786055798535,22.7759604372089,12.1155678887156));
#47324=CARTESIAN_POINT('Ctrl Pts',(-26.6776342334082,22.772045646765,12.1158182782911));
#47325=CARTESIAN_POINT('Ctrl Pts',(-26.6771099412237,22.7699416933075,12.1159527556708));
#47326=CARTESIAN_POINT('Ctrl Pts',(-26.6756785804037,22.764222334813,12.1163180729448));
#47327=CARTESIAN_POINT('Ctrl Pts',(-26.6747673585438,22.7606079575401,12.1165486715475));
#47328=CARTESIAN_POINT('Ctrl Pts',(-26.6704082102087,22.7434430065688,12.1176425752836));
#47329=CARTESIAN_POINT('Ctrl Pts',(-26.6668783238818,22.729913116428,12.1185011866327));
#47330=CARTESIAN_POINT('Ctrl Pts',(-26.6023500718809,22.4890090273683,12.1337311398228));
#47331=CARTESIAN_POINT('Ctrl Pts',(-26.5166957068614,22.2689287919727,12.1467538621821));
#47332=CARTESIAN_POINT('Ctrl Pts',(-26.3872188411653,22.0206374073645,12.1624033714415));
#47333=CARTESIAN_POINT('Ctrl Pts',(-26.365814291604,21.9815867958034,12.1648936692625));
#47334=CARTESIAN_POINT('Ctrl Pts',(-26.3218448765043,21.9051696694215,12.169843502498));
#47335=CARTESIAN_POINT('Ctrl Pts',(-26.2993164889924,21.8677933218009,12.1723021272307));
#47336=CARTESIAN_POINT('Ctrl Pts',(-26.2074364487072,21.7221319934775,12.1820652117813));
#47337=CARTESIAN_POINT('Ctrl Pts',(-26.1323960706743,21.6175909896871,12.1894823789752));
#47338=CARTESIAN_POINT('Ctrl Pts',(-26.0196937486545,21.4789022087681,12.2001246831744));
#47339=CARTESIAN_POINT('Ctrl Pts',(-25.9871671719643,21.4407315689241,12.2031448655017));
#47340=CARTESIAN_POINT('Ctrl Pts',(-25.949984013577,21.3991043302083,12.2065481457253));
#47341=CARTESIAN_POINT('Ctrl Pts',(-25.9461922119889,21.3948818402269,12.2068946453915));
#47342=CARTESIAN_POINT('Ctrl Pts',(-25.9398125734151,21.3878152134252,12.2074767085759));
#47343=CARTESIAN_POINT('Ctrl Pts',(-25.9372307535791,21.3849656415856,12.2077120176891));
#47344=CARTESIAN_POINT('Ctrl Pts',(-25.9321345786174,21.3793611505714,12.2081759993136));
#47345=CARTESIAN_POINT('Ctrl Pts',(-25.9296205280847,21.3766059616061,12.2084046587037));
#47346=CARTESIAN_POINT('Ctrl Pts',(-25.9248308360907,21.3713751266576,12.2088398554652));
#47347=CARTESIAN_POINT('Ctrl Pts',(-25.9225560903345,21.3688986641579,12.2090463544947));
#47348=CARTESIAN_POINT('Ctrl Pts',(-25.9173721197974,21.3632726961371,12.2095165281168));
#47349=CARTESIAN_POINT('Ctrl Pts',(-25.9144604817994,21.3601254317544,12.2097803057697));
#47350=CARTESIAN_POINT('Ctrl Pts',(-25.9056018801081,21.3505881919075,12.2105819398645));
#47351=CARTESIAN_POINT('Ctrl Pts',(-25.8996352635171,21.3442165986662,12.2111206400982));
#47352=CARTESIAN_POINT('Ctrl Pts',(-25.8573492692387,21.2994266215793,12.2149299389543));
#47353=CARTESIAN_POINT('Ctrl Pts',(-25.8201170672009,21.2618847535737,12.2182400626652));
#47354=CARTESIAN_POINT('Ctrl Pts',(-25.7791231222399,21.2225349509252,12.2218415425201));
#47355=CARTESIAN_POINT('Ctrl Pts',(-25.7762611316239,21.2197978640303,12.2220927589447));
#47356=CARTESIAN_POINT('Ctrl Pts',(-25.7704725834773,21.214282333108,12.222600415537));
#47357=CARTESIAN_POINT('Ctrl Pts',(-25.7675458381388,21.2115040971712,12.2228568637536));
#47358=CARTESIAN_POINT('Ctrl Pts',(-25.7612489424562,21.20554916379,12.223408125095));
#47359=CARTESIAN_POINT('Ctrl Pts',(-25.757877150235,21.2023742224283,12.2237030101263));
#47360=CARTESIAN_POINT('Ctrl Pts',(-25.739702778606,21.185334663516,12.2252908785694));
#47361=CARTESIAN_POINT('Ctrl Pts',(-25.7247766684107,21.1716029869927,12.2265892702901));
#47362=CARTESIAN_POINT('Ctrl Pts',(-25.5921579310663,21.0518883099257,12.2380760900638));
#47363=CARTESIAN_POINT('Ctrl Pts',(-25.4669449838263,20.9545868539293,12.2485985469542));
#47364=CARTESIAN_POINT('Ctrl Pts',(-25.2648736593938,20.8201781199876,12.2649589977585));
#47365=CARTESIAN_POINT('Ctrl Pts',(-25.1928377896861,20.7762400367263,12.2706786860824));
#47366=CARTESIAN_POINT('Ctrl Pts',(-25.041142966112,20.6916967788872,12.2824202997753));
#47367=CARTESIAN_POINT('Ctrl Pts',(-24.961346124519,20.6514749368908,12.2884353794428));
#47368=CARTESIAN_POINT('Ctrl Pts',(-24.8186968933982,20.5868604905487,12.2988054439178));
#47369=CARTESIAN_POINT('Ctrl Pts',(-24.7565565401166,20.5610259632413,12.3032009527136));
#47370=CARTESIAN_POINT('Ctrl Pts',(-24.6758411530252,20.5303964774462,12.3087166962151));
#47371=CARTESIAN_POINT('Ctrl Pts',(-24.6579736138941,20.5237967865959,12.3099257187946));
#47372=CARTESIAN_POINT('Ctrl Pts',(-24.629123999839,20.5134303995344,12.3118574602161));
#47373=CARTESIAN_POINT('Ctrl Pts',(-24.6181785439863,20.5095640653729,12.3125856660564));
#47374=CARTESIAN_POINT('Ctrl Pts',(-24.604853644943,20.5049380507426,12.3134662809272));
#47375=CARTESIAN_POINT('Ctrl Pts',(-24.6024940900343,20.5041219535735,12.3136219949516));
#47376=CARTESIAN_POINT('Ctrl Pts',(-24.5979343269672,20.502550802634,12.3139224713079));
#47377=CARTESIAN_POINT('Ctrl Pts',(-24.5957342461335,20.501795387774,12.3140672550178));
#47378=CARTESIAN_POINT('Ctrl Pts',(-24.5917667988417,20.5004379340799,12.3143279908685));
#47379=CARTESIAN_POINT('Ctrl Pts',(-24.5899997313038,20.4998350505195,12.3144439933168));
#47380=CARTESIAN_POINT('Ctrl Pts',(-24.5861997338368,20.4985422627508,12.3146931777323));
#47381=CARTESIAN_POINT('Ctrl Pts',(-24.5841666438308,20.4978528560306,12.3148263295532));
#47382=CARTESIAN_POINT('Ctrl Pts',(-24.5786889771401,20.4960015178925,12.3151846267146));
#47383=CARTESIAN_POINT('Ctrl Pts',(-24.5752431078255,20.4948433779504,12.3154095460663));
#47384=CARTESIAN_POINT('Ctrl Pts',(-24.5593846199082,20.489543264315,12.3164425037078));
#47385=CARTESIAN_POINT('Ctrl Pts',(-24.5469485767194,20.4854710062822,12.3172464554461));
#47386=CARTESIAN_POINT('Ctrl Pts',(-24.3219204603616,20.4132987560228,12.3316900410853));
#47387=CARTESIAN_POINT('Ctrl Pts',(-24.1028062393352,20.367381367461,12.3441087266092));
#47388=CARTESIAN_POINT('Ctrl Pts',(-23.7215469805187,20.3280845937371,12.3655245211381));
#47389=CARTESIAN_POINT('Ctrl Pts',(-23.5614261096603,20.3235547241923,12.3744600407154));
#47390=CARTESIAN_POINT('Ctrl Pts',(-23.2985467387886,20.3356899466087,12.3896711794525));
#47391=CARTESIAN_POINT('Ctrl Pts',(-23.1957509916258,20.3453978096635,12.3957532966788));
#47392=CARTESIAN_POINT('Ctrl Pts',(-23.0732888433141,20.3629269431133,12.4032355469154));
#47393=CARTESIAN_POINT('Ctrl Pts',(-23.0530012514773,20.366028936896,12.4044828325208));
#47394=CARTESIAN_POINT('Ctrl Pts',(-23.0283513415207,20.3700392486509,12.40600815405));
#47395=CARTESIAN_POINT('Ctrl Pts',(-23.0239591568385,20.3707631605499,12.4062803205849));
#47396=CARTESIAN_POINT('Ctrl Pts',(-23.0154619082103,20.3721817512233,12.4068076049703));
#47397=CARTESIAN_POINT('Ctrl Pts',(-23.0113566608171,20.3728752898889,12.407062686113));
#47398=CARTESIAN_POINT('Ctrl Pts',(-23.004264407641,20.3740875923032,12.4075039509772));
#47399=CARTESIAN_POINT('Ctrl Pts',(-23.0012767615913,20.3746026206426,12.4076900154793));
#47400=CARTESIAN_POINT('Ctrl Pts',(-22.9950932391181,20.3756775602188,12.4080754862494));
#47401=CARTESIAN_POINT('Ctrl Pts',(-22.9918974736278,20.376238083294,12.4082749118398));
#47402=CARTESIAN_POINT('Ctrl Pts',(-22.9841524875955,20.3776085784464,12.4087587266489));
#47403=CARTESIAN_POINT('Ctrl Pts',(-22.979604161271,20.3784235087177,12.4090432737982));
#47404=CARTESIAN_POINT('Ctrl Pts',(-22.9626533053871,20.381498258876,12.4101053173987));
#47405=CARTESIAN_POINT('Ctrl Pts',(-22.9502624427238,20.3838210421242,12.4108848216122));
#47406=CARTESIAN_POINT('Ctrl Pts',(-22.7364428133157,20.4252036471991,12.4243917703911));
#47407=CARTESIAN_POINT('Ctrl Pts',(-22.5392238224086,20.4833308445629,12.4377511318064));
#47408=CARTESIAN_POINT('Ctrl Pts',(-22.2406549010072,20.6032745929559,12.4593115707154));
#47409=CARTESIAN_POINT('Ctrl Pts',(-22.1348554122537,20.6526027074621,12.4672263787619));
#47410=CARTESIAN_POINT('Ctrl Pts',(-21.9341842687456,20.7597812776515,12.4826089448638));
#47411=CARTESIAN_POINT('Ctrl Pts',(-21.839155552902,20.8170206399463,12.490068812216));
#47412=CARTESIAN_POINT('Ctrl Pts',(-21.7063826128123,20.9066387868157,12.5005810887377));
#47413=CARTESIAN_POINT('Ctrl Pts',(-21.666140502092,20.9351669979323,12.5037794508485));
#47414=CARTESIAN_POINT('Ctrl Pts',(-21.6127181364398,20.9749125594687,12.5080254340408));
#47415=CARTESIAN_POINT('Ctrl Pts',(-21.5989520999209,20.9853271603682,12.509119551023));
#47416=CARTESIAN_POINT('Ctrl Pts',(-21.5767375633319,21.0024157792196,12.5108842518007));
#47417=CARTESIAN_POINT('Ctrl Pts',(-21.5682378613114,21.0090222584145,12.5115592429886));
#47418=CARTESIAN_POINT('Ctrl Pts',(-21.5578518357827,21.0171787100422,12.5123836001375));
#47419=CARTESIAN_POINT('Ctrl Pts',(-21.5559340971832,21.0186882917684,12.5125357961856));
#47420=CARTESIAN_POINT('Ctrl Pts',(-21.5522235596711,21.0216159396864,12.5128302343398));
#47421=CARTESIAN_POINT('Ctrl Pts',(-21.5504305518047,21.0230337369886,12.5129724954674));
#47422=CARTESIAN_POINT('Ctrl Pts',(-21.5471777093889,21.025611508625,12.5132305489739));
#47423=CARTESIAN_POINT('Ctrl Pts',(-21.5457173781071,21.0267708382392,12.5133463868667));
#47424=CARTESIAN_POINT('Ctrl Pts',(-21.5427770551997,21.0291092683387,12.5135795965207));
#47425=CARTESIAN_POINT('Ctrl Pts',(-21.5412971018857,21.0302884001681,12.5136969650987));
#47426=CARTESIAN_POINT('Ctrl Pts',(-21.5370592654813,21.0336709422632,12.5140330150882));
#47427=CARTESIAN_POINT('Ctrl Pts',(-21.5343039519525,21.0358775899822,12.5142514631643));
#47428=CARTESIAN_POINT('Ctrl Pts',(-21.5223843282463,21.0454558460183,12.5151963278757));
#47429=CARTESIAN_POINT('Ctrl Pts',(-21.5132566327153,21.0528731843108,12.5159194858819));
#47430=CARTESIAN_POINT('Ctrl Pts',(-21.3563303303913,21.1818272285785,12.5283495115638));
#47431=CARTESIAN_POINT('Ctrl Pts',(-21.2195794964766,21.3162606172501,12.5391504471633));
#47432=CARTESIAN_POINT('Ctrl Pts',(-20.9903022205163,21.5857788536466,12.5589624169127));
#47433=CARTESIAN_POINT('Ctrl Pts',(-20.8945581547298,21.7172801882064,12.5679706498143));
#47434=CARTESIAN_POINT('Ctrl Pts',(-20.7617980318484,21.9319995698742,12.5824019411968));
#47435=CARTESIAN_POINT('Ctrl Pts',(-20.717689296962,22.0105107508227,12.587623528924));
#47436=CARTESIAN_POINT('Ctrl Pts',(-20.6494720373039,22.1448112179258,12.5965492698235));
#47437=CARTESIAN_POINT('Ctrl Pts',(-20.6235495138283,22.1996225076053,12.6001900340611));
#47438=CARTESIAN_POINT('Ctrl Pts',(-20.5958701184,22.2626926937489,12.6043886788086));
#47439=CARTESIAN_POINT('Ctrl Pts',(-20.5925800320215,22.270268483766,12.604893150223));
#47440=CARTESIAN_POINT('Ctrl Pts',(-20.5876460778569,22.2817500607094,12.6056579544832));
#47441=CARTESIAN_POINT('Ctrl Pts',(-20.585980714297,22.2856466201438,12.6059175527084));
#47442=CARTESIAN_POINT('Ctrl Pts',(-20.5831330501037,22.2923460175987,12.606363960622));
#47443=CARTESIAN_POINT('Ctrl Pts',(-20.5819470209457,22.2951472727647,12.6065506428963));
#47444=CARTESIAN_POINT('Ctrl Pts',(-20.5795156630539,22.3009125634801,12.6069349053137));
#47445=CARTESIAN_POINT('Ctrl Pts',(-20.5782708002299,22.3038767911598,12.6071325010944));
#47446=CARTESIAN_POINT('Ctrl Pts',(-20.5752894628311,22.3110057195054,12.6076077837204));
#47447=CARTESIAN_POINT('Ctrl Pts',(-20.5735572985081,22.3151722059563,12.6078856168021));
#47448=CARTESIAN_POINT('Ctrl Pts',(-20.5672799860644,22.3303613431314,12.6088986821734));
#47449=CARTESIAN_POINT('Ctrl Pts',(-20.5627873098702,22.3414054519858,12.6096356920489));
#47450=CARTESIAN_POINT('Ctrl Pts',(-20.490634976463,22.5216327031507,12.6216701657291));
#47451=CARTESIAN_POINT('Ctrl Pts',(-20.4373937635843,22.6961987116296,12.6334605310436));
#47452=CARTESIAN_POINT('Ctrl Pts',(-20.3609520345424,23.0525449577599,12.6577402115178));
#47453=CARTESIAN_POINT('Ctrl Pts',(-20.3379099518835,23.233708399093,12.6701849705025));
#47454=CARTESIAN_POINT('Ctrl Pts',(-20.3274463490543,23.4843597546447,12.6870431640661));
#47455=CARTESIAN_POINT('Ctrl Pts',(-20.3267737977663,23.5529631390126,12.691617217088));
#47456=CARTESIAN_POINT('Ctrl Pts',(-20.3294308078937,23.6730532495847,12.6995021584923));
#47457=CARTESIAN_POINT('Ctrl Pts',(-20.3318059406975,23.7245361972825,12.702843025759));
#47458=CARTESIAN_POINT('Ctrl Pts',(-20.3371353598512,23.8004508379356,12.7076902575868));
#47459=CARTESIAN_POINT('Ctrl Pts',(-20.3391361261755,23.8249390292553,12.7092416503787));
#47460=CARTESIAN_POINT('Ctrl Pts',(-20.3418129815249,23.8536523182508,12.7110444950601));
#47461=CARTESIAN_POINT('Ctrl Pts',(-20.3422175922927,23.8579010416103,12.7113108456383));
#47462=CARTESIAN_POINT('Ctrl Pts',(-20.3428515430429,23.8644207513634,12.7117189093962));
#47463=CARTESIAN_POINT('Ctrl Pts',(-20.3430748555175,23.8666922980998,12.7118609619231));
#47464=CARTESIAN_POINT('Ctrl Pts',(-20.3434671296774,23.8706394604394,12.7121075859598));
#47465=CARTESIAN_POINT('Ctrl Pts',(-20.3436349911408,23.872315176779,12.7122122197958));
#47466=CARTESIAN_POINT('Ctrl Pts',(-20.3439895206481,23.8758265956148,12.7124313361009));
#47467=CARTESIAN_POINT('Ctrl Pts',(-20.344176451152,23.8776622641649,12.7125458031708));
#47468=CARTESIAN_POINT('Ctrl Pts',(-20.3447017422782,23.8827770663358,12.7128645255361));
#47469=CARTESIAN_POINT('Ctrl Pts',(-20.3450435590845,23.8860558547835,12.7130685845681));
#47470=CARTESIAN_POINT('Ctrl Pts',(-20.3464322409015,23.8991811136403,12.7138844511981));
#47471=CARTESIAN_POINT('Ctrl Pts',(-20.3475194668355,23.9090233949306,12.7144939975841));
#47472=CARTESIAN_POINT('Ctrl Pts',(-20.3672564239271,24.0804516579629,12.7250739949944));
#47473=CARTESIAN_POINT('Ctrl Pts',(-20.3980709234063,24.2404282105695,12.7343821353934));
#47474=CARTESIAN_POINT('Ctrl Pts',(-20.4970029778575,24.6035472928319,12.7555675281017));
#47475=CARTESIAN_POINT('Ctrl Pts',(-20.57351985322,24.8035775947017,12.767311198549));
#47476=CARTESIAN_POINT('Ctrl Pts',(-20.6899952423621,25.0359123478748,12.7822730444915));
#47477=CARTESIAN_POINT('Ctrl Pts',(-20.7116108294858,25.076807435002,12.7849579853745));
#47478=CARTESIAN_POINT('Ctrl Pts',(-20.7735420016451,25.188110006927,12.7924274003587));
#47479=CARTESIAN_POINT('Ctrl Pts',(-20.8156452075056,25.2574782148758,12.7972664319348));
#47480=CARTESIAN_POINT('Ctrl Pts',(-20.8659756517482,25.3337549097732,12.8028289148867));
#47481=CARTESIAN_POINT('Ctrl Pts',(-20.8716745181362,25.3423024535066,12.8034557509153));
#47482=CARTESIAN_POINT('Ctrl Pts',(-20.8800047573507,25.3546681952177,12.8043677556763));
#47483=CARTESIAN_POINT('Ctrl Pts',(-20.8826036961857,25.3585082528822,12.8046516963061));
#47484=CARTESIAN_POINT('Ctrl Pts',(-20.8871309996156,25.3651665596831,12.805145292631));
#47485=CARTESIAN_POINT('Ctrl Pts',(-20.889055577722,25.3679873846459,12.8053548042458));
#47486=CARTESIAN_POINT('Ctrl Pts',(-20.8927664866768,25.3734078822708,12.8057581688946));
#47487=CARTESIAN_POINT('Ctrl Pts',(-20.8945521588681,25.3760080031228,12.8059519966835));
#47488=CARTESIAN_POINT('Ctrl Pts',(-20.8987703739668,25.3821308728561,12.8064092361674));
#47489=CARTESIAN_POINT('Ctrl Pts',(-20.9012061204963,25.3856513985918,12.8066727700542));
#47490=CARTESIAN_POINT('Ctrl Pts',(-20.9084278456946,25.396045054318,12.8074526750924));
#47491=CARTESIAN_POINT('Ctrl Pts',(-20.9132335830471,25.4029043528635,12.8079698026508));
#47492=CARTESIAN_POINT('Ctrl Pts',(-20.9559430687199,25.4633613587537,12.8125493692115));
#47493=CARTESIAN_POINT('Ctrl Pts',(-20.99544707207,25.5158046202051,12.8166734275706));
#47494=CARTESIAN_POINT('Ctrl Pts',(-21.0470671302845,25.5801452224494,12.8219333810961));
#47495=CARTESIAN_POINT('Ctrl Pts',(-21.0577144579651,25.5932051557233,12.823011781879));
#47496=CARTESIAN_POINT('Ctrl Pts',(-21.1120645111481,25.6588131658551,12.8284839033188));
#47497=CARTESIAN_POINT('Ctrl Pts',(-21.157326104986,25.7100420716934,12.8329362703006));
#47498=CARTESIAN_POINT('Ctrl Pts',(-21.3691530469982,25.9349585076166,12.8533021167513));
#47499=CARTESIAN_POINT('Ctrl Pts',(-21.5532223144827,26.0910929051231,12.8698242664419));
#47500=CARTESIAN_POINT('Ctrl Pts',(-21.8257229957743,26.2741851064674,12.8917570024975));
#47501=CARTESIAN_POINT('Ctrl Pts',(-21.9005000118894,26.3201135486168,12.8975393880501));
#47502=CARTESIAN_POINT('Ctrl Pts',(-22.0064189117119,26.3793560330567,12.9053200910249));
#47503=CARTESIAN_POINT('Ctrl Pts',(-22.0360307734183,26.3953151948964,12.9074527034947));
#47504=CARTESIAN_POINT('Ctrl Pts',(-22.0689351273279,26.4123895115327,12.9097713274644));
#47505=CARTESIAN_POINT('Ctrl Pts',(-22.0719843072135,26.4139655760787,12.909985710627));
#47506=CARTESIAN_POINT('Ctrl Pts',(-22.0750360153462,26.4155367745564,12.9101997884793));
#47507=CARTESIAN_POINT('Origin',(-23.5502525316942,23.5502525316942,-77.3107734492734));
#47508=CARTESIAN_POINT('',(-22.0750358569346,26.4155366929967,14.4063516850465));
#47509=CARTESIAN_POINT('',(-22.0750361586249,26.4155368483246,14.1564144975666));
#47510=CARTESIAN_POINT('',(-22.0750360153461,26.4155367745563,-77.3107734492734));
#47511=CARTESIAN_POINT('',(-26.7696996717685,23.55268397525,13.5607719477124));
#47512=CARTESIAN_POINT('Ctrl Pts',(-22.0750358569346,26.4155366929967,14.4063516850465));
#47513=CARTESIAN_POINT('Ctrl Pts',(-22.0142029387246,26.3842163316414,14.4023201504987));
#47514=CARTESIAN_POINT('Ctrl Pts',(-21.9543647139263,26.3509572618314,14.398227214807));
#47515=CARTESIAN_POINT('Ctrl Pts',(-21.8858777544244,26.309981299096,14.393373398924));
#47516=CARTESIAN_POINT('Ctrl Pts',(-21.876173242285,26.3041052504215,14.3926815727776));
#47517=CARTESIAN_POINT('Ctrl Pts',(-21.8627333518613,26.2958701480209,14.391717741403));
#47518=CARTESIAN_POINT('Ctrl Pts',(-21.8589714132938,26.2935544209534,14.3914473313953));
#47519=CARTESIAN_POINT('Ctrl Pts',(-21.8525014599586,26.289553361214,14.3909811845128));
#47520=CARTESIAN_POINT('Ctrl Pts',(-21.8497911566245,26.2878717250761,14.3907855842914));
#47521=CARTESIAN_POINT('Ctrl Pts',(-21.8443523023718,26.2844859378319,14.3903924045676));
#47522=CARTESIAN_POINT('Ctrl Pts',(-21.8416237983045,26.282781719637,14.3901948227564));
#47523=CARTESIAN_POINT('Ctrl Pts',(-21.8352447242594,26.2787840725517,14.3897320997684));
#47524=CARTESIAN_POINT('Ctrl Pts',(-21.8315962020672,26.2764874022365,14.3894668385383));
#47525=CARTESIAN_POINT('Ctrl Pts',(-21.8203912081306,26.2694026544044,14.3886503201982));
#47526=CARTESIAN_POINT('Ctrl Pts',(-21.8128501033255,26.2645904597913,14.3880981663744));
#47527=CARTESIAN_POINT('Ctrl Pts',(-21.795561470701,26.2534565234525,14.3868262066001));
#47528=CARTESIAN_POINT('Ctrl Pts',(-21.7858279406812,26.2471133730282,14.386105603215));
#47529=CARTESIAN_POINT('Ctrl Pts',(-21.6948388319251,26.1871141160455,14.3793267854803));
#47530=CARTESIAN_POINT('Ctrl Pts',(-21.6160277185812,26.1298591097764,14.3731326656458));
#47531=CARTESIAN_POINT('Ctrl Pts',(-21.3777677906952,25.9397037040801,14.3533442272863));
#47532=CARTESIAN_POINT('Ctrl Pts',(-21.228496030504,25.7949336836897,14.3393137962258));
#47533=CARTESIAN_POINT('Ctrl Pts',(-20.9729332779317,25.4941192319451,14.312605572933));
#47534=CARTESIAN_POINT('Ctrl Pts',(-20.8643316980723,25.3410734617185,14.2999919058949));
#47535=CARTESIAN_POINT('Ctrl Pts',(-20.7638035359656,25.1694969332139,14.2874597656363));
#47536=CARTESIAN_POINT('Ctrl Pts',(-20.7580295377401,25.1595198181541,14.2867365329266));
#47537=CARTESIAN_POINT('Ctrl Pts',(-20.7505711484559,25.1464711822578,14.2857980237518));
#47538=CARTESIAN_POINT('Ctrl Pts',(-20.7488381516001,25.1434277572542,14.2855796492051));
#47539=CARTESIAN_POINT('Ctrl Pts',(-20.7461792578408,25.1387405538515,14.2852441362653));
#47540=CARTESIAN_POINT('Ctrl Pts',(-20.74524984442,25.1370987895604,14.2851267698875));
#47541=CARTESIAN_POINT('Ctrl Pts',(-20.7434045438485,25.1338324676737,14.2848935710443));
#47542=CARTESIAN_POINT('Ctrl Pts',(-20.7424886304771,25.1322079405363,14.2847777375001));
#47543=CARTESIAN_POINT('Ctrl Pts',(-20.7404487755772,25.1285825609308,14.2845195698734));
#47544=CARTESIAN_POINT('Ctrl Pts',(-20.7393255634705,25.1265813071948,14.2843772835931));
#47545=CARTESIAN_POINT('Ctrl Pts',(-20.7360479501751,25.1207268626825,14.2839616944584));
#47546=CARTESIAN_POINT('Ctrl Pts',(-20.7338993163644,25.1168704232009,14.283688764218));
#47547=CARTESIAN_POINT('Ctrl Pts',(-20.7183477544624,25.0888225678663,14.2817096529921));
#47548=CARTESIAN_POINT('Ctrl Pts',(-20.7052482630322,25.0644629724648,14.2800226743612));
#47549=CARTESIAN_POINT('Ctrl Pts',(-20.664292738755,24.9858944774439,14.2746732289151));
#47550=CARTESIAN_POINT('Ctrl Pts',(-20.6376586840455,24.9310601991972,14.2710776878622));
#47551=CARTESIAN_POINT('Ctrl Pts',(-20.5781852625296,24.7992262530383,14.2626795273687));
#47552=CARTESIAN_POINT('Ctrl Pts',(-20.5467581430206,24.7216372389472,14.2579295961377));
#47553=CARTESIAN_POINT('Ctrl Pts',(-20.4197022219535,24.3690867322549,14.236843177525));
#47554=CARTESIAN_POINT('Ctrl Pts',(-20.3585748744525,24.083186927155,14.220921035406));
#47555=CARTESIAN_POINT('Ctrl Pts',(-20.3361369641207,23.7861042929074,14.2031944560384));
#47556=CARTESIAN_POINT('Ctrl Pts',(-20.3356405929824,23.7792394689123,14.2027842941276));
#47557=CARTESIAN_POINT('Ctrl Pts',(-20.3320804218505,23.7277077480629,14.199701138409));
#47558=CARTESIAN_POINT('Ctrl Pts',(-20.329925849144,23.6829847202599,14.197001456098));
#47559=CARTESIAN_POINT('Ctrl Pts',(-20.3285001242239,23.6307794450926,14.1938177493432));
#47560=CARTESIAN_POINT('Ctrl Pts',(-20.3283224380257,23.6233252958665,14.1933623963767));
#47561=CARTESIAN_POINT('Ctrl Pts',(-20.3280802255348,23.6114318043876,14.1926346109333));
#47562=CARTESIAN_POINT('Ctrl Pts',(-20.3279990010389,23.6069927983005,14.1923627029124));
#47563=CARTESIAN_POINT('Ctrl Pts',(-20.3278718584805,23.5991594156847,14.1918823813876));
#47564=CARTESIAN_POINT('Ctrl Pts',(-20.3278221302239,23.5957651007533,14.1916740878192));
#47565=CARTESIAN_POINT('Ctrl Pts',(-20.3277313807123,23.5888218300205,14.1912476741062));
#47566=CARTESIAN_POINT('Ctrl Pts',(-20.3276908589237,23.5852728733397,14.1910295385679));
#47567=CARTESIAN_POINT('Ctrl Pts',(-20.3276055013191,23.5765324405043,14.1904918636632));
#47568=CARTESIAN_POINT('Ctrl Pts',(-20.3275673476793,23.5713409223144,14.1901721148989));
#47569=CARTESIAN_POINT('Ctrl Pts',(-20.3274671817358,23.551034614295,14.1889199023045));
#47570=CARTESIAN_POINT('Ctrl Pts',(-20.3274989602527,23.5359197440218,14.1879844988325));
#47571=CARTESIAN_POINT('Ctrl Pts',(-20.3278410569835,23.4984810054802,14.1856590880073));
#47572=CARTESIAN_POINT('Ctrl Pts',(-20.3282770255972,23.4761593411435,14.1842651746593));
#47573=CARTESIAN_POINT('Ctrl Pts',(-20.3308692773963,23.3895437727808,14.1788264848373));
#47574=CARTESIAN_POINT('Ctrl Pts',(-20.3347183828118,23.3253191327741,14.1747294990411));
#47575=CARTESIAN_POINT('Ctrl Pts',(-20.3559535923923,23.0894682226301,14.159441181367));
#47576=CARTESIAN_POINT('Ctrl Pts',(-20.3851850358819,22.919219894207,14.1479097030004));
#47577=CARTESIAN_POINT('Ctrl Pts',(-20.4748604529884,22.5683899019768,14.1234310472453));
#47578=CARTESIAN_POINT('Ctrl Pts',(-20.5379632463702,22.3891269208478,14.1105036297968));
#47579=CARTESIAN_POINT('Ctrl Pts',(-20.6206722335937,22.2072037891786,14.0975185927279));
#47580=CARTESIAN_POINT('Ctrl Pts',(-20.6249180211257,22.1979808673657,14.0968607419501));
#47581=CARTESIAN_POINT('Ctrl Pts',(-20.6312920980296,22.1843052775927,14.0958861210028));
#47582=CARTESIAN_POINT('Ctrl Pts',(-20.6333871039772,22.1798372692728,14.095567830644));
#47583=CARTESIAN_POINT('Ctrl Pts',(-20.6388460096187,22.1682643186375,14.0947437762109));
#47584=CARTESIAN_POINT('Ctrl Pts',(-20.6422256790694,22.1611667946765,14.0942387630755));
#47585=CARTESIAN_POINT('Ctrl Pts',(-20.6485904205377,22.1479254621691,14.0932973803523));
#47586=CARTESIAN_POINT('Ctrl Pts',(-20.65156911397,22.1417786544757,14.0928606946515));
#47587=CARTESIAN_POINT('Ctrl Pts',(-20.6659446374602,22.1123522018075,14.0907718448422));
#47588=CARTESIAN_POINT('Ctrl Pts',(-20.6776029134701,22.0892002867249,14.0891334579532));
#47589=CARTESIAN_POINT('Ctrl Pts',(-20.6916659282011,22.0620920860076,14.0872233110144));
#47590=CARTESIAN_POINT('Ctrl Pts',(-20.6938009864599,22.0579980453084,14.0869350520328));
#47591=CARTESIAN_POINT('Ctrl Pts',(-20.6970445483644,22.0518108825075,14.0864997711836));
#47592=CARTESIAN_POINT('Ctrl Pts',(-20.6981465613434,22.0497143928483,14.0863523399783));
#47593=CARTESIAN_POINT('Ctrl Pts',(-20.7001231142995,22.0459642062422,14.0860887289006));
#47594=CARTESIAN_POINT('Ctrl Pts',(-20.7009967817137,22.0443100582717,14.0859724937168));
#47595=CARTESIAN_POINT('Ctrl Pts',(-20.7028626321134,22.0407848084066,14.0857248630409));
#47596=CARTESIAN_POINT('Ctrl Pts',(-20.7038552166992,22.0389139286229,14.085593494046));
#47597=CARTESIAN_POINT('Ctrl Pts',(-20.7065403114797,22.0338649374345,14.0852390984224));
#47598=CARTESIAN_POINT('Ctrl Pts',(-20.7082363111876,22.0306886698904,14.0850162945565));
#47599=CARTESIAN_POINT('Ctrl Pts',(-20.7165772309169,22.0151306097217,14.083925619333));
#47600=CARTESIAN_POINT('Ctrl Pts',(-20.7232978947413,22.0027892774572,14.0830625231316));
#47601=CARTESIAN_POINT('Ctrl Pts',(-20.7808326367159,21.8987625413934,14.0758016036561));
#47602=CARTESIAN_POINT('Ctrl Pts',(-20.8360172527908,21.8095522273518,14.0696681703263));
#47603=CARTESIAN_POINT('Ctrl Pts',(-21.0534455835168,21.4936217155273,14.0477028509342));
#47604=CARTESIAN_POINT('Ctrl Pts',(-21.2405378733918,21.2855213774076,14.0326427488444));
#47605=CARTESIAN_POINT('Ctrl Pts',(-21.4935371483055,21.0685146515761,14.0133691735308));
#47606=CARTESIAN_POINT('Ctrl Pts',(-21.5358923678211,21.0340145179315,14.0101780259796));
#47607=CARTESIAN_POINT('Ctrl Pts',(-21.5877667381218,20.9939100239729,14.0062987698934));
#47608=CARTESIAN_POINT('Ctrl Pts',(-21.5964652349386,20.9872557112353,14.0056492446608));
#47609=CARTESIAN_POINT('Ctrl Pts',(-21.6107810217605,20.9764194243055,14.004581726848));
#47610=CARTESIAN_POINT('Ctrl Pts',(-21.6163783650655,20.9722111609891,14.0041646988256));
#47611=CARTESIAN_POINT('Ctrl Pts',(-21.6232806609528,20.9670569198226,14.0036508678575));
#47612=CARTESIAN_POINT('Ctrl Pts',(-21.6245726948971,20.9660936112792,14.003554702478));
#47613=CARTESIAN_POINT('Ctrl Pts',(-21.6359532425114,20.9576218311829,14.0027078122126));
#47614=CARTESIAN_POINT('Ctrl Pts',(-21.646084797578,20.9501715807355,14.0019549558013));
#47615=CARTESIAN_POINT('Ctrl Pts',(-21.6663118637146,20.9354792174883,14.0004538864889));
#47616=CARTESIAN_POINT('Ctrl Pts',(-21.6764061639986,20.9282358061763,13.9997057398887));
#47617=CARTESIAN_POINT('Ctrl Pts',(-21.7050352449431,20.9079420707142,13.9975863359687));
#47618=CARTESIAN_POINT('Ctrl Pts',(-21.7236659136074,20.8950288700357,13.9962099967602));
#47619=CARTESIAN_POINT('Ctrl Pts',(-21.7478252255627,20.8786582832595,13.9944283321966));
#47620=CARTESIAN_POINT('Ctrl Pts',(-21.7532305976075,20.8750194223027,13.9940299032102));
#47621=CARTESIAN_POINT('Ctrl Pts',(-21.7618191635952,20.8692754309997,13.9933971402388));
#47622=CARTESIAN_POINT('Ctrl Pts',(-21.7649951450718,20.867159505001,13.9931632141525));
#47623=CARTESIAN_POINT('Ctrl Pts',(-21.7709384547064,20.8632151335043,13.9927255782272));
#47624=CARTESIAN_POINT('Ctrl Pts',(-21.7737048643314,20.8613853075095,13.9925219207325));
#47625=CARTESIAN_POINT('Ctrl Pts',(-21.7798559893114,20.8573303172754,13.9920691895597));
#47626=CARTESIAN_POINT('Ctrl Pts',(-21.7832420808177,20.8551072598312,13.9918200371894));
#47627=CARTESIAN_POINT('Ctrl Pts',(-21.7930556697901,20.8486908262629,13.9910981348271));
#47628=CARTESIAN_POINT('Ctrl Pts',(-21.7994939335048,20.8445140393466,13.9906247647078));
#47629=CARTESIAN_POINT('Ctrl Pts',(-21.8140502001286,20.8351444503609,13.9895550295402));
#47630=CARTESIAN_POINT('Ctrl Pts',(-21.8221766720946,20.829965000995,13.988958171381));
#47631=CARTESIAN_POINT('Ctrl Pts',(-21.8479172651009,20.8137209890315,13.9870686642779));
#47632=CARTESIAN_POINT('Ctrl Pts',(-21.865615069884,20.8027906423523,13.9857710707288));
#47633=CARTESIAN_POINT('Ctrl Pts',(-21.9335037294335,20.7617644644939,13.9807985796295));
#47634=CARTESIAN_POINT('Ctrl Pts',(-21.9844026697482,20.7328679495321,13.9770806831924));
#47635=CARTESIAN_POINT('Ctrl Pts',(-22.1560416723955,20.6415125656399,13.9645712027929));
#47636=CARTESIAN_POINT('Ctrl Pts',(-22.2799326049921,20.5853120393978,13.955578953587));
#47637=CARTESIAN_POINT('Ctrl Pts',(-22.6424802050175,20.4477524270943,13.9295302587125));
#47638=CARTESIAN_POINT('Ctrl Pts',(-22.8876373274337,20.3863139622003,13.9121720158848));
#47639=CARTESIAN_POINT('Ctrl Pts',(-23.1748392305863,20.3492209013376,13.8935462908562));
#47640=CARTESIAN_POINT('Ctrl Pts',(-23.2123098729675,20.3450483706583,13.8911506329103));
#47641=CARTESIAN_POINT('Ctrl Pts',(-23.2550616990382,20.3410458749905,13.8884629654269));
#47642=CARTESIAN_POINT('Ctrl Pts',(-23.2602775465681,20.3405703820042,13.8881358344852));
#47643=CARTESIAN_POINT('Ctrl Pts',(-23.267919245985,20.3398925201727,13.8876577114698));
#47644=CARTESIAN_POINT('Ctrl Pts',(-23.2703441707893,20.3396801843727,13.8875061598264));
#47645=CARTESIAN_POINT('Ctrl Pts',(-23.2746461757725,20.3393083951692,13.887237600054));
#47646=CARTESIAN_POINT('Ctrl Pts',(-23.2765231559845,20.3391478401191,13.8871205293738));
#47647=CARTESIAN_POINT('Ctrl Pts',(-23.2804519716744,20.3388152428964,13.8868756983626));
#47648=CARTESIAN_POINT('Ctrl Pts',(-23.2825038269735,20.3386435216736,13.886747956634));
#47649=CARTESIAN_POINT('Ctrl Pts',(-23.2878823905409,20.3381985761827,13.8864134246947));
#47650=CARTESIAN_POINT('Ctrl Pts',(-23.2912093721805,20.3379285527289,13.8862068159993));
#47651=CARTESIAN_POINT('Ctrl Pts',(-23.3058454254889,20.3367635517003,13.8852992891703));
#47652=CARTESIAN_POINT('Ctrl Pts',(-23.3171589388607,20.3359231079811,13.8846014193999));
#47653=CARTESIAN_POINT('Ctrl Pts',(-23.4003215549433,20.3301866184262,13.8794967475945));
#47654=CARTESIAN_POINT('Ctrl Pts',(-23.4723185991867,20.3276399420705,13.8752153897253));
#47655=CARTESIAN_POINT('Ctrl Pts',(-23.6262441031167,20.3273578574963,13.8662424030426));
#47656=CARTESIAN_POINT('Ctrl Pts',(-23.708122373949,20.3303296445114,13.8615780794641));
#47657=CARTESIAN_POINT('Ctrl Pts',(-23.813873754763,20.3382120504177,13.8555983608753));
#47658=CARTESIAN_POINT('Ctrl Pts',(-23.8379242001918,20.3402766388643,13.8542414652921));
#47659=CARTESIAN_POINT('Ctrl Pts',(-23.882403491687,20.3445988348472,13.8517343230038));
#47660=CARTESIAN_POINT('Ctrl Pts',(-23.9028382276226,20.3467820357256,13.8505833995107));
#47661=CARTESIAN_POINT('Ctrl Pts',(-23.9409629459315,20.3512244112206,13.8484358561341));
#47662=CARTESIAN_POINT('Ctrl Pts',(-23.9586577249909,20.3534352482392,13.847439004415));
#47663=CARTESIAN_POINT('Ctrl Pts',(-24.1283313643118,20.3760665151404,13.8378727126086));
#47664=CARTESIAN_POINT('Ctrl Pts',(-24.2786838517404,20.4071622407372,13.8293258207096));
#47665=CARTESIAN_POINT('Ctrl Pts',(-24.4793288046129,20.4638342830492,13.8173441072551));
#47666=CARTESIAN_POINT('Ctrl Pts',(-24.532017389905,20.4801877695452,13.8141432478161));
#47667=CARTESIAN_POINT('Ctrl Pts',(-24.5921841713001,20.5005695899272,13.8104114546292));
#47668=CARTESIAN_POINT('Ctrl Pts',(-24.6000992854876,20.5032852888936,13.8099189870317));
#47669=CARTESIAN_POINT('Ctrl Pts',(-24.6741445200517,20.5290131970191,13.8052972259453));
#47670=CARTESIAN_POINT('Ctrl Pts',(-24.7395145871519,20.5541425619747,13.8011058131571));
#47671=CARTESIAN_POINT('Ctrl Pts',(-24.8126316594597,20.5850199824749,13.7962716496089));
#47672=CARTESIAN_POINT('Ctrl Pts',(-24.8212364254666,20.5886980290668,13.795700420637));
#47673=CARTESIAN_POINT('Ctrl Pts',(-24.8338915575807,20.5941726874369,13.7948568376666));
#47674=CARTESIAN_POINT('Ctrl Pts',(-24.8379544872731,20.5959402821696,13.7945854765096));
#47675=CARTESIAN_POINT('Ctrl Pts',(-24.8451224463395,20.599076328802,13.794105792078));
#47676=CARTESIAN_POINT('Ctrl Pts',(-24.8482289903587,20.6004413192632,13.7938975877226));
#47677=CARTESIAN_POINT('Ctrl Pts',(-24.8541990411662,20.6030757683909,13.7934968640113));
#47678=CARTESIAN_POINT('Ctrl Pts',(-24.8570628657015,20.6043445011304,13.7933043697752));
#47679=CARTESIAN_POINT('Ctrl Pts',(-24.8631730047553,20.6070620805576,13.7928930980925));
#47680=CARTESIAN_POINT('Ctrl Pts',(-24.8664187784382,20.6085121265914,13.7926742795595));
#47681=CARTESIAN_POINT('Ctrl Pts',(-24.8787750519438,20.6140568224138,13.7918399375391));
#47682=CARTESIAN_POINT('Ctrl Pts',(-24.8878688241608,20.6181884156609,13.7912231419522));
#47683=CARTESIAN_POINT('Ctrl Pts',(-24.9089483486993,20.6278839966976,13.789786933533));
#47684=CARTESIAN_POINT('Ctrl Pts',(-24.9209193141783,20.6334795305002,13.7889664351532));
#47685=CARTESIAN_POINT('Ctrl Pts',(-24.961578138116,20.6527900754657,13.7861627847028));
#47686=CARTESIAN_POINT('Ctrl Pts',(-24.9900965539964,20.6668556240136,13.7841675045569));
#47687=CARTESIAN_POINT('Ctrl Pts',(-25.1130481097952,20.7297753579528,13.7754370093258));
#47688=CARTESIAN_POINT('Ctrl Pts',(-25.205230498133,20.7828592847096,13.768555680825));
#47689=CARTESIAN_POINT('Ctrl Pts',(-25.3395228773174,20.8693046200107,13.7580228292325));
#47690=CARTESIAN_POINT('Ctrl Pts',(-25.3837047379595,20.8993238824793,13.7544701571006));
#47691=CARTESIAN_POINT('Ctrl Pts',(-25.6649041785372,21.1007775946131,13.7313137978281));
#47692=CARTESIAN_POINT('Ctrl Pts',(-25.8783906368783,21.3027068378809,13.7110146864788));
#47693=CARTESIAN_POINT('Ctrl Pts',(-26.0706194607177,21.541752987898,13.6916071686117));
#47694=CARTESIAN_POINT('Ctrl Pts',(-26.0794596300327,21.5528964428244,13.6907120177312));
#47695=CARTESIAN_POINT('Ctrl Pts',(-26.0912801569453,21.5680011020296,13.6895119044692));
#47696=CARTESIAN_POINT('Ctrl Pts',(-26.0943254086276,21.5719109736385,13.6892024384589));
#47697=CARTESIAN_POINT('Ctrl Pts',(-26.0988354045288,21.5777290998046,13.6887437122166));
#47698=CARTESIAN_POINT('Ctrl Pts',(-26.1003070323245,21.5796319713211,13.6885939630911));
#47699=CARTESIAN_POINT('Ctrl Pts',(-26.1029217449372,21.583020729207,13.6883277832372));
#47700=CARTESIAN_POINT('Ctrl Pts',(-26.1040656629729,21.5845059642209,13.6882112928368));
#47701=CARTESIAN_POINT('Ctrl Pts',(-26.1064855165773,21.5876535199874,13.687964786936));
#47702=CARTESIAN_POINT('Ctrl Pts',(-26.1077611236758,21.5893160830153,13.6878347950183));
#47703=CARTESIAN_POINT('Ctrl Pts',(-26.1111634413813,21.5937594622139,13.6874879461592));
#47704=CARTESIAN_POINT('Ctrl Pts',(-26.113287251615,21.5965425114927,13.6872712959045));
#47705=CARTESIAN_POINT('Ctrl Pts',(-26.1232505719789,21.6096426925679,13.6862542533915));
#47706=CARTESIAN_POINT('Ctrl Pts',(-26.1310324927651,21.6200037733788,13.6854578923549));
#47707=CARTESIAN_POINT('Ctrl Pts',(-26.3141792691389,21.8669384693518,13.6666605042191));
#47708=CARTESIAN_POINT('Ctrl Pts',(-26.4563944933373,22.1264394265528,13.6507663448529));
#47709=CARTESIAN_POINT('Ctrl Pts',(-26.5793638075808,22.4488230248718,13.6313490032783));
#47710=CARTESIAN_POINT('Ctrl Pts',(-26.5962319125702,22.4963685335879,13.6284962472395));
#47711=CARTESIAN_POINT('Ctrl Pts',(-26.618021047271,22.5626853976568,13.6245160554373));
#47712=CARTESIAN_POINT('Ctrl Pts',(-26.6238992846075,22.5811353396411,13.6234086281098));
#47713=CARTESIAN_POINT('Ctrl Pts',(-26.6431807950287,22.6435945291476,13.6196572815646));
#47714=CARTESIAN_POINT('Ctrl Pts',(-26.6558075343745,22.6878362453225,13.6169961035464));
#47715=CARTESIAN_POINT('Ctrl Pts',(-26.674571957731,22.7593505421771,13.6126768553445));
#47716=CARTESIAN_POINT('Ctrl Pts',(-26.6813095879346,22.786459707332,13.6110355537942));
#47717=CARTESIAN_POINT('Ctrl Pts',(-26.6902151184922,22.824391525728,13.6087316088405));
#47718=CARTESIAN_POINT('Ctrl Pts',(-26.6926812263959,22.8351433505509,13.608077730291));
#47719=CARTESIAN_POINT('Ctrl Pts',(-26.7068008428178,22.89818621722,13.6042384998317));
#47720=CARTESIAN_POINT('Ctrl Pts',(-26.7172036412301,22.9507461764746,13.6010163749191));
#47721=CARTESIAN_POINT('Ctrl Pts',(-26.7277779746316,23.0121759259912,13.5972178307639));
#47722=CARTESIAN_POINT('Ctrl Pts',(-26.7292295042233,23.0208190799182,13.5966826337563));
#47723=CARTESIAN_POINT('Ctrl Pts',(-26.7313397112716,23.0337059602368,13.5958835179731));
#47724=CARTESIAN_POINT('Ctrl Pts',(-26.7320251997566,23.0379453064432,13.5956204523088));
#47725=CARTESIAN_POINT('Ctrl Pts',(-26.7332324337978,23.0455072324914,13.595150877286));
#47726=CARTESIAN_POINT('Ctrl Pts',(-26.733757456428,23.0488292889921,13.5949444724148));
#47727=CARTESIAN_POINT('Ctrl Pts',(-26.734762120129,23.0552514364337,13.5945452307467));
#47728=CARTESIAN_POINT('Ctrl Pts',(-26.7352424372382,23.0583514190571,13.5943524156855));
#47729=CARTESIAN_POINT('Ctrl Pts',(-26.7362724017622,23.06506359927,13.5939347071687));
#47730=CARTESIAN_POINT('Ctrl Pts',(-26.7368204334175,23.0686760370997,13.5937097626457));
#47731=CARTESIAN_POINT('Ctrl Pts',(-26.7381354263979,23.0774445520917,13.5931634152084));
#47732=CARTESIAN_POINT('Ctrl Pts',(-26.7388960214375,23.0826015606422,13.5928418105684));
#47733=CARTESIAN_POINT('Ctrl Pts',(-26.7409282409558,23.096615946823,13.5919670585872));
#47734=CARTESIAN_POINT('Ctrl Pts',(-26.7421754859368,23.1054767630348,13.5914131392337));
#47735=CARTESIAN_POINT('Ctrl Pts',(-26.7632251569263,23.259670090473,13.5817590082109));
#47736=CARTESIAN_POINT('Ctrl Pts',(-26.7731168665485,23.4061570475411,13.5723436394165));
#47737=CARTESIAN_POINT('Ctrl Pts',(-26.7730015348059,23.552787377377,13.5626736252116));
#47738=CARTESIAN_POINT('Ctrl Pts',(-22.075954775016,26.4137025163198,13.1538544762662));
#47739=CARTESIAN_POINT('Ctrl Pts',(-22.7503891714052,26.7532021541,13.2004027990139));
#47740=CARTESIAN_POINT('Ctrl Pts',(-24.6803998219367,27.0228698900686,13.3132467588865));
#47741=CARTESIAN_POINT('Ctrl Pts',(-26.5420719176933,25.3662309742614,13.4488859160352));
#47742=CARTESIAN_POINT('Ctrl Pts',(-26.7722508965562,23.9227962910001,13.5379767504363));
#47743=CARTESIAN_POINT('Ctrl Pts',(-26.7696996717685,23.55268397525,13.5607719477124));
#47744=CARTESIAN_POINT('Ctrl Pts',(-22.0750360153462,26.4155367745564,12.9101997884793));
#47745=CARTESIAN_POINT('Ctrl Pts',(-22.0760890146292,26.4160789203968,12.9102736565607));
#47746=CARTESIAN_POINT('Ctrl Pts',(-22.0771423149283,26.4166204868775,12.9103474882914));
#47747=CARTESIAN_POINT('Ctrl Pts',(-22.080292118416,26.4182377998639,12.9105681034007));
#47748=CARTESIAN_POINT('Ctrl Pts',(-22.0823895089747,26.4193118307784,12.9107147784804));
#47749=CARTESIAN_POINT('Ctrl Pts',(-22.0859959120397,26.4211536064108,12.9109665878938));
#47750=CARTESIAN_POINT('Ctrl Pts',(-22.0875043503513,26.4219224617247,12.9110717929643));
#47751=CARTESIAN_POINT('Ctrl Pts',(-22.0906273645983,26.4235111718192,12.911289360033));
#47752=CARTESIAN_POINT('Ctrl Pts',(-22.0922420215443,26.4243308524444,12.9114017108153));
#47753=CARTESIAN_POINT('Ctrl Pts',(-22.0961688624288,26.4263201525001,12.9116746204702));
#47754=CARTESIAN_POINT('Ctrl Pts',(-22.0984817724824,26.4274883474522,12.9118350888975));
#47755=CARTESIAN_POINT('Ctrl Pts',(-22.1071737908921,26.4318653265521,12.9124371119949));
#47756=CARTESIAN_POINT('Ctrl Pts',(-22.1135622114161,26.4350557273318,12.9128775142274));
#47757=CARTESIAN_POINT('Ctrl Pts',(-22.2186652618329,26.4871088486118,12.9200899813498));
#47758=CARTESIAN_POINT('Ctrl Pts',(-22.3198230877258,26.5309066618636,12.9265539691476));
#47759=CARTESIAN_POINT('Ctrl Pts',(-22.646552758391,26.6528913009366,12.9465547385214));
#47760=CARTESIAN_POINT('Ctrl Pts',(-22.8786490089429,26.7112650881736,12.95954054459));
#47761=CARTESIAN_POINT('Ctrl Pts',(-23.2571233585094,26.7628443401656,12.981298976024));
#47762=CARTESIAN_POINT('Ctrl Pts',(-23.4002906374693,26.7727010411547,12.989646639936));
#47763=CARTESIAN_POINT('Ctrl Pts',(-23.5582327225904,26.7730257484614,12.9991906553933));
#47764=CARTESIAN_POINT('Ctrl Pts',(-23.572838277788,26.772956483871,13.0000762728136));
#47765=CARTESIAN_POINT('Ctrl Pts',(-23.5982051001567,26.7726637343368,13.0016199073607));
#47766=CARTESIAN_POINT('Ctrl Pts',(-23.6089667321288,26.7724856154407,13.0022764992294));
#47767=CARTESIAN_POINT('Ctrl Pts',(-23.6243836749394,26.7721531864686,13.0032196501878));
#47768=CARTESIAN_POINT('Ctrl Pts',(-23.6290399388523,26.7720426862119,13.0035048334076));
#47769=CARTESIAN_POINT('Ctrl Pts',(-23.6371305274474,26.7718331345573,13.0040009394578));
#47770=CARTESIAN_POINT('Ctrl Pts',(-23.6405649722276,26.7717386840511,13.0042117174934));
#47771=CARTESIAN_POINT('Ctrl Pts',(-23.6471269694284,26.7715477210139,13.0046147885852));
#47772=CARTESIAN_POINT('Ctrl Pts',(-23.6502545471095,26.7714521452262,13.0048070519888));
#47773=CARTESIAN_POINT('Ctrl Pts',(-23.6575601431357,26.7712182430976,13.0052565098583));
#47774=CARTESIAN_POINT('Ctrl Pts',(-23.661738034727,26.77107634244,13.0055138163829));
#47775=CARTESIAN_POINT('Ctrl Pts',(-23.6760973293548,26.7705606613993,13.0063991160263));
#47776=CARTESIAN_POINT('Ctrl Pts',(-23.6862771491114,26.770146732281,13.0070283692233));
#47777=CARTESIAN_POINT('Ctrl Pts',(-23.7927449871843,26.7653117697163,13.0136269347085));
#47778=CARTESIAN_POINT('Ctrl Pts',(-23.88878116157,26.7566217633932,13.01973004565));
#47779=CARTESIAN_POINT('Ctrl Pts',(-24.2839818400787,26.7029088247568,13.0455108545032));
#47780=CARTESIAN_POINT('Ctrl Pts',(-24.5764414252619,26.6201841589304,13.0663676788769));
#47781=CARTESIAN_POINT('Ctrl Pts',(-24.884913959955,26.4838533225825,13.088838012318));
#47782=CARTESIAN_POINT('Ctrl Pts',(-24.9165942187286,26.4692327078018,13.0911490913798));
#47783=CARTESIAN_POINT('Ctrl Pts',(-25.0103204564478,26.4241171910422,13.0979845306184));
#47784=CARTESIAN_POINT('Ctrl Pts',(-25.0716339465085,26.3921351250051,13.1024537884725));
#47785=CARTESIAN_POINT('Ctrl Pts',(-25.141478640888,26.3527939668892,13.1075023968045));
#47786=CARTESIAN_POINT('Ctrl Pts',(-25.1510535519037,26.3473358569926,13.1081935486535));
#47787=CARTESIAN_POINT('Ctrl Pts',(-25.1634851680768,26.3401645579504,13.109089471001));
#47788=CARTESIAN_POINT('Ctrl Pts',(-25.1663673317343,26.3384959942831,13.109297081865));
#47789=CARTESIAN_POINT('Ctrl Pts',(-25.171025855392,26.3357893971026,13.1096324790693));
#47790=CARTESIAN_POINT('Ctrl Pts',(-25.1728038073268,26.3347541304295,13.1097604451286));
#47791=CARTESIAN_POINT('Ctrl Pts',(-25.1762083808187,26.3327673457519,13.1100054065509));
#47792=CARTESIAN_POINT('Ctrl Pts',(-25.1778351541235,26.3318161065444,13.1101224192288));
#47793=CARTESIAN_POINT('Ctrl Pts',(-25.181564554116,26.3296309858585,13.1103905941957));
#47794=CARTESIAN_POINT('Ctrl Pts',(-25.1836666204961,26.3283961421954,13.1105416933428));
#47795=CARTESIAN_POINT('Ctrl Pts',(-25.1902967095267,26.3244912181555,13.1110180990837));
#47796=CARTESIAN_POINT('Ctrl Pts',(-25.1948196313349,26.3218124264839,13.1113428386469));
#47797=CARTESIAN_POINT('Ctrl Pts',(-25.2321372554418,26.2995867976096,13.1140202517666));
#47798=CARTESIAN_POINT('Ctrl Pts',(-25.2645905381461,26.2794686542824,13.1163362588766));
#47799=CARTESIAN_POINT('Ctrl Pts',(-25.3059258847923,26.2528160661589,13.1192802894086));
#47800=CARTESIAN_POINT('Ctrl Pts',(-25.3151409452556,26.2468072733507,13.1199362335319));
#47801=CARTESIAN_POINT('Ctrl Pts',(-25.5777990613099,26.0736146373945,13.1386272168853));
#47802=CARTESIAN_POINT('Ctrl Pts',(-25.8064128810081,25.8714792483265,13.1548754515252));
#47803=CARTESIAN_POINT('Ctrl Pts',(-26.0665089258595,25.5662011070761,13.177727505221));
#47804=CARTESIAN_POINT('Ctrl Pts',(-26.1262497525851,25.4892808652838,13.1833574408407));
#47805=CARTESIAN_POINT('Ctrl Pts',(-26.2189731775053,25.3580307571731,13.1928676325672));
#47806=CARTESIAN_POINT('Ctrl Pts',(-26.2539955130713,25.3052183546097,13.1966699218102));
#47807=CARTESIAN_POINT('Ctrl Pts',(-26.2918666083502,25.2442832987771,13.2010432347214));
#47808=CARTESIAN_POINT('Ctrl Pts',(-26.2962684182788,25.2371386374133,13.2015557908225));
#47809=CARTESIAN_POINT('Ctrl Pts',(-26.302841328439,25.2263761191056,13.2023275972631));
#47810=CARTESIAN_POINT('Ctrl Pts',(-26.3050333350008,25.2227710187991,13.2025860784789));
#47811=CARTESIAN_POINT('Ctrl Pts',(-26.308792179942,25.2165615694073,13.2030312078137));
#47812=CARTESIAN_POINT('Ctrl Pts',(-26.3103624291416,25.2139592829061,13.2032177305503));
#47813=CARTESIAN_POINT('Ctrl Pts',(-26.3135896837366,25.2085937895922,13.2036022621594));
#47814=CARTESIAN_POINT('Ctrl Pts',(-26.315246230912,25.2058303120063,13.2038002875527));
#47815=CARTESIAN_POINT('Ctrl Pts',(-26.3192259095221,25.1991687174601,13.2042775838279));
#47816=CARTESIAN_POINT('Ctrl Pts',(-26.3215449527221,25.195268176491,13.2045570036859));
#47817=CARTESIAN_POINT('Ctrl Pts',(-26.3286420848976,25.1832734742668,13.2054161140473));
#47818=CARTESIAN_POINT('Ctrl Pts',(-26.3333929758748,25.1751633517673,13.205996793527));
#47819=CARTESIAN_POINT('Ctrl Pts',(-26.3887460526593,25.0797166095454,13.2128286304378));
#47820=CARTESIAN_POINT('Ctrl Pts',(-26.4352486133737,24.9900788273038,13.2192269687596));
#47821=CARTESIAN_POINT('Ctrl Pts',(-26.4918457529391,24.867191615932,13.2279890482217));
#47822=CARTESIAN_POINT('Ctrl Pts',(-26.5057250071247,24.8357413679618,13.2302304104488));
#47823=CARTESIAN_POINT('Ctrl Pts',(-26.6176680867532,24.5706787501887,13.2491074577465));
#47824=CARTESIAN_POINT('Ctrl Pts',(-26.6883655152247,24.3264806809558,13.2665125650853));
#47825=CARTESIAN_POINT('Ctrl Pts',(-26.7493352292583,23.9581643472272,13.2914621421967));
#47826=CARTESIAN_POINT('Ctrl Pts',(-26.7623088510815,23.838737874378,13.2993398647134));
#47827=CARTESIAN_POINT('Ctrl Pts',(-26.7689189370707,23.7125603529907,13.3072585501932));
#47828=CARTESIAN_POINT('Ctrl Pts',(-26.7692300990929,23.7062675314069,13.3076524153361));
#47829=CARTESIAN_POINT('Ctrl Pts',(-26.7696461141904,23.6973224745093,13.3082107353359));
#47830=CARTESIAN_POINT('Ctrl Pts',(-26.769766145568,23.6946710114692,13.3083760374412));
#47831=CARTESIAN_POINT('Ctrl Pts',(-26.7699670758576,23.6901077358023,13.3086601930956));
#47832=CARTESIAN_POINT('Ctrl Pts',(-26.7700495477356,23.688195996838,13.308779135795));
#47833=CARTESIAN_POINT('Ctrl Pts',(-26.7702043966908,23.6845307120772,13.3090069829559));
#47834=CARTESIAN_POINT('Ctrl Pts',(-26.7702770439217,23.6827771834125,13.3091159027087));
#47835=CARTESIAN_POINT('Ctrl Pts',(-26.7704449153017,23.6786435324645,13.309372462334));
#47836=CARTESIAN_POINT('Ctrl Pts',(-26.7705389332734,23.6762633582622,13.3095200338033));
#47837=CARTESIAN_POINT('Ctrl Pts',(-26.7708091326994,23.6692250955594,13.3099559505528));
#47838=CARTESIAN_POINT('Ctrl Pts',(-26.7709778479184,23.6645667010217,13.3102438770115));
#47839=CARTESIAN_POINT('Ctrl Pts',(-26.7723687797822,23.6237111620692,13.3127640120366));
#47840=CARTESIAN_POINT('Ctrl Pts',(-26.7729909022866,23.5874943287455,13.3149631334267));
#47841=CARTESIAN_POINT('Ctrl Pts',(-26.7730347348718,23.4490485647083,13.3232625536465));
#47842=CARTESIAN_POINT('Ctrl Pts',(-26.768203290968,23.3468706993055,13.3291653882643));
#47843=CARTESIAN_POINT('Ctrl Pts',(-26.7245388259226,22.8878173385831,13.3553517595979));
#47844=CARTESIAN_POINT('Ctrl Pts',(-26.6311313745349,22.5387659216273,13.3746802204848));
#47845=CARTESIAN_POINT('Ctrl Pts',(-26.4736680397546,22.1937220673131,13.3976168869846));
#47846=CARTESIAN_POINT('Ctrl Pts',(-26.4650289741884,22.175257479284,13.3988556169586));
#47847=CARTESIAN_POINT('Ctrl Pts',(-26.453511735187,22.1512376404951,13.4004822896714));
#47848=CARTESIAN_POINT('Ctrl Pts',(-26.4507916142844,22.1456067763672,13.4008647268163));
#47849=CARTESIAN_POINT('Ctrl Pts',(-26.4465751959254,22.1369429319076,13.4014548734712));
#47850=CARTESIAN_POINT('Ctrl Pts',(-26.4450904736969,22.1339043084132,13.401662178525));
#47851=CARTESIAN_POINT('Ctrl Pts',(-26.4421285801691,22.1278666279533,13.4020747407217));
#47852=CARTESIAN_POINT('Ctrl Pts',(-26.4406515197578,22.1248675210497,13.4022799937911));
#47853=CARTESIAN_POINT('Ctrl Pts',(-26.4373730587202,22.1182367990171,13.4027344995731));
#47854=CARTESIAN_POINT('Ctrl Pts',(-26.4355694692152,22.1146062779029,13.4029838287909));
#47855=CARTESIAN_POINT('Ctrl Pts',(-26.4303643763494,22.1041781551492,13.4037013577848));
#47856=CARTESIAN_POINT('Ctrl Pts',(-26.4269456845719,22.0973892061115,13.4041701609419));
#47857=CARTESIAN_POINT('Ctrl Pts',(-26.404204648655,22.052624271167,13.4072725205479));
#47858=CARTESIAN_POINT('Ctrl Pts',(-26.3841555797846,22.0150241039054,13.4099316447025));
#47859=CARTESIAN_POINT('Ctrl Pts',(-26.3231253757619,21.9058388102278,13.4178160986461));
#47860=CARTESIAN_POINT('Ctrl Pts',(-26.2801372682049,21.835420857111,13.4231120440113));
#47861=CARTESIAN_POINT('Ctrl Pts',(-26.0690549651572,21.5177360086348,13.4480027342875));
#47862=CARTESIAN_POINT('Ctrl Pts',(-25.869805189754,21.293014867854,13.4686949538292));
#47863=CARTESIAN_POINT('Ctrl Pts',(-25.5748066288183,21.0412262900228,13.4943371255897));
#47864=CARTESIAN_POINT('Ctrl Pts',(-25.5047699577869,20.9862913336202,13.50011089492));
#47865=CARTESIAN_POINT('Ctrl Pts',(-25.4273499192802,20.9305838730474,13.5060901028499));
#47866=CARTESIAN_POINT('Ctrl Pts',(-25.4221462904076,20.9268630750309,13.5064900938947));
#47867=CARTESIAN_POINT('Ctrl Pts',(-25.4149139261054,20.9217241272722,13.50704337492));
#47868=CARTESIAN_POINT('Ctrl Pts',(-25.4128946285229,20.920292815675,13.5071975667357));
#47869=CARTESIAN_POINT('Ctrl Pts',(-25.4094208628145,20.9178365605755,13.507462326605));
#47870=CARTESIAN_POINT('Ctrl Pts',(-25.4079671951702,20.9168104955782,13.5075729723746));
#47871=CARTESIAN_POINT('Ctrl Pts',(-25.4049625146326,20.9146933808315,13.5078013657549));
#47872=CARTESIAN_POINT('Ctrl Pts',(-25.4034113914225,20.9136024981986,13.50791910133));
#47873=CARTESIAN_POINT('Ctrl Pts',(-25.3997671861678,20.9110443854657,13.5081953138826));
#47874=CARTESIAN_POINT('Ctrl Pts',(-25.3976733142084,20.9095782714579,13.5083537134177));
#47875=CARTESIAN_POINT('Ctrl Pts',(-25.3908665849309,20.90482430731,13.5088676527205));
#47876=CARTESIAN_POINT('Ctrl Pts',(-25.3861466434397,20.9015465466883,13.5092225007244));
#47877=CARTESIAN_POINT('Ctrl Pts',(-25.2511836191136,20.8083556309474,13.5193263145242));
#47878=CARTESIAN_POINT('Ctrl Pts',(-25.1144805777191,20.728130748235,13.5284293807049));
#47879=CARTESIAN_POINT('Ctrl Pts',(-24.6685525390206,20.5088410142806,13.5564727088257));
#47880=CARTESIAN_POINT('Ctrl Pts',(-24.3430778271196,20.4082470927213,13.5748796902867));
#47881=CARTESIAN_POINT('Ctrl Pts',(-23.9881273839712,20.3573255984267,13.5965702006371));
#47882=CARTESIAN_POINT('Ctrl Pts',(-23.9683236576181,20.3546722568234,13.5977844985711));
#47883=CARTESIAN_POINT('Ctrl Pts',(-23.9423401133947,20.3514365969539,13.5993835152735));
#47884=CARTESIAN_POINT('Ctrl Pts',(-23.9361811806791,20.3506876967339,13.5997629588706));
#47885=CARTESIAN_POINT('Ctrl Pts',(-23.9266715942994,20.3495592282707,13.6003495006943));
#47886=CARTESIAN_POINT('Ctrl Pts',(-23.9233224195391,20.3491671232868,13.6005562024325));
#47887=CARTESIAN_POINT('Ctrl Pts',(-23.9166508749906,20.3483966639437,13.6009682088982));
#47888=CARTESIAN_POINT('Ctrl Pts',(-23.913328519315,20.3480182225128,13.6011735106033));
#47889=CARTESIAN_POINT('Ctrl Pts',(-23.9060424069379,20.3471997640689,13.6016240298211));
#47890=CARTESIAN_POINT('Ctrl Pts',(-23.9020784146447,20.3467619330852,13.6018693160478));
#47891=CARTESIAN_POINT('Ctrl Pts',(-23.8907590929466,20.3455329540814,13.6025702655101));
#47892=CARTESIAN_POINT('Ctrl Pts',(-23.8834018738874,20.3447597764809,13.6030264953344));
#47893=CARTESIAN_POINT('Ctrl Pts',(-23.8668828130589,20.3430812568386,13.6040523096185));
#47894=CARTESIAN_POINT('Ctrl Pts',(-23.8577196509148,20.3421898313867,13.60462233003));
#47895=CARTESIAN_POINT('Ctrl Pts',(-23.6527883668902,20.3231394437953,13.6173934318721));
#47896=CARTESIAN_POINT('Ctrl Pts',(-23.4558072222142,20.3228965132843,13.6301731140655));
#47897=CARTESIAN_POINT('Ctrl Pts',(-23.0307682693458,20.3613249300302,13.658721940921));
#47898=CARTESIAN_POINT('Ctrl Pts',(-22.8043635805349,20.4065650467632,13.6745575817468));
#47899=CARTESIAN_POINT('Ctrl Pts',(-22.5201407739078,20.4958183519919,13.6941524000776));
#47900=CARTESIAN_POINT('Ctrl Pts',(-22.4562171518796,20.5181267906043,13.6985349497666));
#47901=CARTESIAN_POINT('Ctrl Pts',(-22.3802338547722,20.5473602443118,13.7036760110389));
#47902=CARTESIAN_POINT('Ctrl Pts',(-22.3674604181117,20.5523685069095,13.7045378970302));
#47903=CARTESIAN_POINT('Ctrl Pts',(-22.3512821714888,20.558831241537,13.7056261486081));
#47904=CARTESIAN_POINT('Ctrl Pts',(-22.3478476047982,20.5602101152792,13.7058569855419));
#47905=CARTESIAN_POINT('Ctrl Pts',(-22.3424103242237,20.5624039011325,13.7062221086276));
#47906=CARTESIAN_POINT('Ctrl Pts',(-22.340406055446,20.5632149120328,13.70635663071));
#47907=CARTESIAN_POINT('Ctrl Pts',(-22.3368467890316,20.5646593100148,13.7065953977134));
#47908=CARTESIAN_POINT('Ctrl Pts',(-22.3352914789837,20.565291891738,13.706699690941));
#47909=CARTESIAN_POINT('Ctrl Pts',(-22.3316789953829,20.5667644662592,13.7069418333288));
#47910=CARTESIAN_POINT('Ctrl Pts',(-22.3296221991345,20.5676053699772,13.7070796260104));
#47911=CARTESIAN_POINT('Ctrl Pts',(-22.3237978543273,20.5699936376472,13.7074696187913));
#47912=CARTESIAN_POINT('Ctrl Pts',(-22.3200323499259,20.5715460245026,13.7077215133138));
#47913=CARTESIAN_POINT('Ctrl Pts',(-22.2971763626606,20.5810194883337,13.7092490701682));
#47914=CARTESIAN_POINT('Ctrl Pts',(-22.2781589322225,20.5891171618776,13.7105141367341));
#47915=CARTESIAN_POINT('Ctrl Pts',(-22.2214289227027,20.613920370587,13.7142738294222));
#47916=CARTESIAN_POINT('Ctrl Pts',(-22.1839564161904,20.6311680827679,13.7167384920901));
#47917=CARTESIAN_POINT('Ctrl Pts',(-22.0764232280724,20.6831876948469,13.7237854978818));
#47918=CARTESIAN_POINT('Ctrl Pts',(-22.0072812818265,20.7197976411985,13.728284664035));
#47919=CARTESIAN_POINT('Ctrl Pts',(-21.6375772939359,20.9331301008273,13.7525249196615));
#47920=CARTESIAN_POINT('Ctrl Pts',(-21.3659135028519,21.1551898971024,13.7713129099303));
#47921=CARTESIAN_POINT('Ctrl Pts',(-21.1158498725972,21.4382286045062,13.7940422155562));
#47922=CARTESIAN_POINT('Ctrl Pts',(-21.096912505344,21.4602563581055,13.7958022358817));
#47923=CARTESIAN_POINT('Ctrl Pts',(-21.0741486228984,21.4874708231131,13.7979671272959));
#47924=CARTESIAN_POINT('Ctrl Pts',(-21.0700360965401,21.4924174123866,13.7983602450613));
#47925=CARTESIAN_POINT('Ctrl Pts',(-21.0632782032856,21.5005955620775,13.7990095732424));
#47926=CARTESIAN_POINT('Ctrl Pts',(-21.0606242452798,21.5038200264582,13.7992654335999));
#47927=CARTESIAN_POINT('Ctrl Pts',(-21.0558519428783,21.5096412273421,13.7997270688794));
#47928=CARTESIAN_POINT('Ctrl Pts',(-21.0537313636026,21.5122361308597,13.799932752758));
#47929=CARTESIAN_POINT('Ctrl Pts',(-21.0492648360855,21.5177191485434,13.8003671572195));
#47930=CARTESIAN_POINT('Ctrl Pts',(-21.0469198359111,21.5206080255684,13.8005959157108));
#47931=CARTESIAN_POINT('Ctrl Pts',(-21.040769208546,21.5282120452587,13.8011977382662));
#47932=CARTESIAN_POINT('Ctrl Pts',(-21.0369718804037,21.532933854591,13.8015711360437));
#47933=CARTESIAN_POINT('Ctrl Pts',(-21.0286167171303,21.5433833378178,13.8023968032338));
#47934=CARTESIAN_POINT('Ctrl Pts',(-21.0240650439164,21.5491158752423,13.8028493175737));
#47935=CARTESIAN_POINT('Ctrl Pts',(-21.0106587592742,21.566118851554,13.8041902215362));
#47936=CARTESIAN_POINT('Ctrl Pts',(-21.0018598479592,21.5774327962996,13.8050808247874));
#47937=CARTESIAN_POINT('Ctrl Pts',(-20.9087485621644,21.698820862043,13.8146194174393));
#47938=CARTESIAN_POINT('Ctrl Pts',(-20.8315597064804,21.8141527200699,13.8235457822466));
#47939=CARTESIAN_POINT('Ctrl Pts',(-20.6746932833012,22.0847779560447,13.8441926274079));
#47940=CARTESIAN_POINT('Ctrl Pts',(-20.599709757958,22.2422978238224,13.8560167135887));
#47941=CARTESIAN_POINT('Ctrl Pts',(-20.4837734195369,22.5472758794155,13.8780734134664));
#47942=CARTESIAN_POINT('Ctrl Pts',(-20.4398502988963,22.6931271115699,13.8882849208496));
#47943=CARTESIAN_POINT('Ctrl Pts',(-20.4054318759038,22.8458097148962,13.8983046391235));
#47944=CARTESIAN_POINT('Ctrl Pts',(-20.4044800493325,22.8500724627846,13.8985838450503));
#47945=CARTESIAN_POINT('Ctrl Pts',(-20.4024435578289,22.859280852079,13.8991858126033));
#47946=CARTESIAN_POINT('Ctrl Pts',(-20.4013618734185,22.8642271524552,13.8995084306072));
#47947=CARTESIAN_POINT('Ctrl Pts',(-20.3984111900931,22.8778739840161,13.9003964833664));
#47948=CARTESIAN_POINT('Ctrl Pts',(-20.3965665477139,22.8865798167594,13.9009607112578));
#47949=CARTESIAN_POINT('Ctrl Pts',(-20.3918123744017,22.9094847047598,13.902438958579));
#47950=CARTESIAN_POINT('Ctrl Pts',(-20.3889624859441,22.9236961489612,13.9033498670902));
#47951=CARTESIAN_POINT('Ctrl Pts',(-20.3854907058621,22.9416357222806,13.9044914169664));
#47952=CARTESIAN_POINT('Ctrl Pts',(-20.384779421142,22.9453460747408,13.9047270702611));
#47953=CARTESIAN_POINT('Ctrl Pts',(-20.3836679842414,22.9511994299092,13.9050981154988));
#47954=CARTESIAN_POINT('Ctrl Pts',(-20.3832634821689,22.9533415875995,13.9052337562961));
#47955=CARTESIAN_POINT('Ctrl Pts',(-20.3825170624198,22.9573165862676,13.9054851699103));
#47956=CARTESIAN_POINT('Ctrl Pts',(-20.3821745637353,22.9591493024321,13.9056009754381));
#47957=CARTESIAN_POINT('Ctrl Pts',(-20.3814161645905,22.96322710267,13.9058583958888));
#47958=CARTESIAN_POINT('Ctrl Pts',(-20.3810010605094,22.9654723265994,13.9059999643676));
#47959=CARTESIAN_POINT('Ctrl Pts',(-20.379800430283,22.9720051489733,13.9064114004878));
#47960=CARTESIAN_POINT('Ctrl Pts',(-20.3790212124724,22.9762939238804,13.9066809068463));
#47961=CARTESIAN_POINT('Ctrl Pts',(-20.3735946130188,23.0065100784415,13.9085755479458));
#47962=CARTESIAN_POINT('Ctrl Pts',(-20.3692563764936,23.0324929774112,13.9101832935549));
#47963=CARTESIAN_POINT('Ctrl Pts',(-20.3585719392816,23.1016984708984,13.9144155976454));
#47964=CARTESIAN_POINT('Ctrl Pts',(-20.3527849295169,23.1450031264455,13.9170123869929));
#47965=CARTESIAN_POINT('Ctrl Pts',(-20.3379678712164,23.2761383443914,13.924756717945));
#47966=CARTESIAN_POINT('Ctrl Pts',(-20.3316639958613,23.3642386013023,13.9297992730091));
#47967=CARTESIAN_POINT('Ctrl Pts',(-20.3210667793382,23.7134220287852,13.9495249199212));
#47968=CARTESIAN_POINT('Ctrl Pts',(-20.3448790640442,23.9743333519304,13.9637765785128));
#47969=CARTESIAN_POINT('Ctrl Pts',(-20.4194232271444,24.3200607830885,13.9844181801597));
#47970=CARTESIAN_POINT('Ctrl Pts',(-20.4428385409979,24.4097132036604,13.9899271140004));
#47971=CARTESIAN_POINT('Ctrl Pts',(-20.4730863232288,24.5079947382254,13.9961869154009));
#47972=CARTESIAN_POINT('Ctrl Pts',(-20.4761389306971,24.5177480474846,13.9968105566313));
#47973=CARTESIAN_POINT('Ctrl Pts',(-20.4804860031172,24.5314089746514,13.997687521106));
#47974=CARTESIAN_POINT('Ctrl Pts',(-20.4817416640941,24.5353289554771,13.9979395658332));
#47975=CARTESIAN_POINT('Ctrl Pts',(-20.4840558789441,24.5425062188146,13.9984017852077));
#47976=CARTESIAN_POINT('Ctrl Pts',(-20.4851121235143,24.5457642448076,13.9986118834421));
#47977=CARTESIAN_POINT('Ctrl Pts',(-20.4871489451164,24.5520129251808,13.9990153776024));
#47978=CARTESIAN_POINT('Ctrl Pts',(-20.4881287137721,24.5550038400616,13.9992087465906));
#47979=CARTESIAN_POINT('Ctrl Pts',(-20.4905962669691,24.5624993440383,13.9996939451103));
#47980=CARTESIAN_POINT('Ctrl Pts',(-20.4920896157727,24.5670020813231,13.9999859584437));
#47981=CARTESIAN_POINT('Ctrl Pts',(-20.4971596543363,24.5821770121503,14.0009719305907));
#47982=CARTESIAN_POINT('Ctrl Pts',(-20.500782279691,24.5928336691238,14.0016674097824));
#47983=CARTESIAN_POINT('Ctrl Pts',(-20.5095058313893,24.6180612201338,14.0033212212832));
#47984=CARTESIAN_POINT('Ctrl Pts',(-20.5146557424052,24.6326147677317,14.0042811721772));
#47985=CARTESIAN_POINT('Ctrl Pts',(-20.5332473982988,24.6839778961395,14.0076902441949));
#47986=CARTESIAN_POINT('Ctrl Pts',(-20.5472553029542,24.7205775306143,14.0101581279805));
#47987=CARTESIAN_POINT('Ctrl Pts',(-20.5940462911039,24.8364567802455,14.0180987416822));
#47988=CARTESIAN_POINT('Ctrl Pts',(-20.6293266849482,24.9146816368908,14.0236524448172));
#47989=CARTESIAN_POINT('Ctrl Pts',(-20.7276360862386,25.1113190746447,14.0381075927319));
#47990=CARTESIAN_POINT('Ctrl Pts',(-20.795009764753,25.2273704780872,14.0471241513402));
#47991=CARTESIAN_POINT('Ctrl Pts',(-20.9781336513916,25.5018414550085,14.0694452821793));
#47992=CARTESIAN_POINT('Ctrl Pts',(-21.1014997962609,25.6545617503964,14.0827769227213));
#47993=CARTESIAN_POINT('Ctrl Pts',(-21.2647199450713,25.8226811401634,14.0978547713474));
#47994=CARTESIAN_POINT('Ctrl Pts',(-21.2919495345811,25.8497435371589,14.1002948863727));
#47995=CARTESIAN_POINT('Ctrl Pts',(-21.3234573829001,25.8799582306063,14.1030274144155));
#47996=CARTESIAN_POINT('Ctrl Pts',(-21.3272661127705,25.8835927684478,14.1033562487614));
#47997=CARTESIAN_POINT('Ctrl Pts',(-21.332852707056,25.8888977658009,14.1038363959952));
#47998=CARTESIAN_POINT('Ctrl Pts',(-21.334623564088,25.8905755417324,14.1039882751632));
#47999=CARTESIAN_POINT('Ctrl Pts',(-21.337765953823,25.8935459954563,14.1042572165494));
#48000=CARTESIAN_POINT('Ctrl Pts',(-21.3391367161578,25.8948394814423,14.1043743419131));
#48001=CARTESIAN_POINT('Ctrl Pts',(-21.3420056925938,25.8975419663331,14.1046190820237));
#48002=CARTESIAN_POINT('Ctrl Pts',(-21.343504117705,25.8989507306498,14.1047466785157));
#48003=CARTESIAN_POINT('Ctrl Pts',(-21.3474300513924,25.9026346758131,14.1050803940657));
#48004=CARTESIAN_POINT('Ctrl Pts',(-21.3498597443817,25.9049075411327,14.1052863332482));
#48005=CARTESIAN_POINT('Ctrl Pts',(-21.3605151682964,25.9148443018117,14.1061869160111));
#48006=CARTESIAN_POINT('Ctrl Pts',(-21.3687775812838,25.9224690078034,14.106878568695));
#48007=CARTESIAN_POINT('Ctrl Pts',(-21.4294746039489,25.9778960292262,14.1119124846623));
#48008=CARTESIAN_POINT('Ctrl Pts',(-21.483439762614,26.0240024568831,14.1161329555529));
#48009=CARTESIAN_POINT('Ctrl Pts',(-21.6538441684543,26.1601183743674,14.1288550348207));
#48010=CARTESIAN_POINT('Ctrl Pts',(-21.774962994599,26.2439707978081,14.1370797444969));
#48011=CARTESIAN_POINT('Ctrl Pts',(-21.9582948740137,26.353139221211,14.1490036783203));
#48012=CARTESIAN_POINT('Ctrl Pts',(-22.0162031362245,26.3852461586997,14.1526987592031));
#48013=CARTESIAN_POINT('Ctrl Pts',(-22.0750361586249,26.4155368483246,14.1564144975666));
#48014=CARTESIAN_POINT('Origin',(-23.5502525316942,23.5502525316942,-77.3107734492734));
#48015=CARTESIAN_POINT('',(-22.0750357147148,26.4155366197736,15.6517373095585));
#48016=CARTESIAN_POINT('',(-22.0750360153461,26.4155367745563,15.4070961373485));
#48017=CARTESIAN_POINT('',(-22.0750360153461,26.4155367745563,-77.3107734492734));
#48018=CARTESIAN_POINT('Ctrl Pts',(-22.0750357147148,26.4155366197736,15.6517373095584));
#48019=CARTESIAN_POINT('Ctrl Pts',(-21.9384970982726,26.3452385072826,15.6430022732087));
#48020=CARTESIAN_POINT('Ctrl Pts',(-21.8070317499559,26.265205804068,15.6345020377301));
#48021=CARTESIAN_POINT('Ctrl Pts',(-21.5085125180744,26.0527684592155,15.6139443619397));
#48022=CARTESIAN_POINT('Ctrl Pts',(-21.3479916439476,25.9127333323856,15.601804203723));
#48023=CARTESIAN_POINT('Ctrl Pts',(-21.1900717776686,25.7447889048543,15.5878405393531));
#48024=CARTESIAN_POINT('Ctrl Pts',(-21.1778231020358,25.7315415234239,15.5867430333099));
#48025=CARTESIAN_POINT('Ctrl Pts',(-21.1618319742737,25.7139525191278,15.5852906974511));
#48026=CARTESIAN_POINT('Ctrl Pts',(-21.1579887839497,25.7097025902243,15.5849401474905));
#48027=CARTESIAN_POINT('Ctrl Pts',(-21.1517223696583,25.7027357204763,15.5843660865009));
#48028=CARTESIAN_POINT('Ctrl Pts',(-21.1492923678544,25.700024870261,15.5841428618572));
#48029=CARTESIAN_POINT('Ctrl Pts',(-21.1446100582099,25.6947835593118,15.583711544893));
#48030=CARTESIAN_POINT('Ctrl Pts',(-21.1423571356176,25.6922536521561,15.5835034788338));
#48031=CARTESIAN_POINT('Ctrl Pts',(-21.137189668407,25.6864324182602,15.5830250086592));
#48032=CARTESIAN_POINT('Ctrl Pts',(-21.1342778660054,25.6831386759572,15.5827544901546));
#48033=CARTESIAN_POINT('Ctrl Pts',(-21.125075366183,25.6726860644171,15.5818966531688));
#48034=CARTESIAN_POINT('Ctrl Pts',(-21.1188097227842,25.6655052940877,15.5813082912353));
#48035=CARTESIAN_POINT('Ctrl Pts',(-21.0953017183096,25.6383213742806,15.5790844626406));
#48036=CARTESIAN_POINT('Ctrl Pts',(-21.0782739784902,25.6181347703707,15.5774401640783));
#48037=CARTESIAN_POINT('Ctrl Pts',(-21.0565590098194,25.5917398774904,15.5752987359473));
#48038=CARTESIAN_POINT('Ctrl Pts',(-21.0516431347031,25.5857203019246,15.5748109338653));
#48039=CARTESIAN_POINT('Ctrl Pts',(-21.0451056786475,25.5776557027918,15.5741581579396));
#48040=CARTESIAN_POINT('Ctrl Pts',(-21.0434647082,25.5756263691432,15.573993959663));
#48041=CARTESIAN_POINT('Ctrl Pts',(-21.038503961822,25.5694763146224,15.5734965332191));
#48042=CARTESIAN_POINT('Ctrl Pts',(-21.0351918804705,25.5653494236394,15.5731630003144));
#48043=CARTESIAN_POINT('Ctrl Pts',(-21.0306543579807,25.559667005313,15.5727040999479));
#48044=CARTESIAN_POINT('Ctrl Pts',(-21.0294201506534,25.5581184610922,15.5725790782482));
#48045=CARTESIAN_POINT('Ctrl Pts',(-21.0238710278884,25.5511428663055,15.5720160630685));
#48046=CARTESIAN_POINT('Ctrl Pts',(-21.0195722305097,25.5457030687679,15.5715774390762));
#48047=CARTESIAN_POINT('Ctrl Pts',(-21.0122285812516,25.5363483468505,15.5708238809107));
#48048=CARTESIAN_POINT('Ctrl Pts',(-21.0091751382871,25.532440171722,15.5705092815528));
#48049=CARTESIAN_POINT('Ctrl Pts',(-21.0036687341064,25.5253587594217,15.5699396368534));
#48050=CARTESIAN_POINT('Ctrl Pts',(-21.0012126474484,25.5221879559001,15.569684712209));
#48051=CARTESIAN_POINT('Ctrl Pts',(-20.9960801319971,25.5155362758231,15.5691502295933));
#48052=CARTESIAN_POINT('Ctrl Pts',(-20.9934048867823,25.5120544999665,15.5688706273495));
#48053=CARTESIAN_POINT('Ctrl Pts',(-20.9783132691954,25.4923297682804,15.5672875939356));
#48054=CARTESIAN_POINT('Ctrl Pts',(-20.9660447883879,25.4759747007311,15.5659786329155));
#48055=CARTESIAN_POINT('Ctrl Pts',(-20.7751907261955,25.2164394501035,15.5452635295142));
#48056=CARTESIAN_POINT('Ctrl Pts',(-20.6314863601676,24.9494983346909,15.5245266860199));
#48057=CARTESIAN_POINT('Ctrl Pts',(-20.4966844908557,24.5844220973162,15.4984908085983));
#48058=CARTESIAN_POINT('Ctrl Pts',(-20.469712358939,24.5010728270338,15.4927055812756));
#48059=CARTESIAN_POINT('Ctrl Pts',(-20.4392428266385,24.3919171950279,15.4854163446113));
#48060=CARTESIAN_POINT('Ctrl Pts',(-20.4326161323492,24.367029225528,15.4837734019697));
#48061=CARTESIAN_POINT('Ctrl Pts',(-20.4239229468351,24.3327316494013,15.4815378631532));
#48062=CARTESIAN_POINT('Ctrl Pts',(-20.421599425109,24.3233889924433,15.4809317992994));
#48063=CARTESIAN_POINT('Ctrl Pts',(-20.4182130136489,24.309507264424,15.4800357214841));
#48064=CARTESIAN_POINT('Ctrl Pts',(-20.4171180768358,24.304976176608,15.4797439360673));
#48065=CARTESIAN_POINT('Ctrl Pts',(-20.4153889809418,24.2977521866913,15.479279870633));
#48066=CARTESIAN_POINT('Ctrl Pts',(-20.4147484567957,24.2950608375608,15.4791072300335));
#48067=CARTESIAN_POINT('Ctrl Pts',(-20.4135590291707,24.2900343830949,15.4787852721389));
#48068=CARTESIAN_POINT('Ctrl Pts',(-20.4130092663402,24.2876994860683,15.4786359055207));
#48069=CARTESIAN_POINT('Ctrl Pts',(-20.412035780863,24.2835442066709,15.4783704268037));
#48070=CARTESIAN_POINT('Ctrl Pts',(-20.4116110342726,24.2817240666976,15.4782542550879));
#48071=CARTESIAN_POINT('Ctrl Pts',(-20.4107888606498,24.2781869563423,15.478028723327));
#48072=CARTESIAN_POINT('Ctrl Pts',(-20.4103912593126,24.276470032606,15.4779193531646));
#48073=CARTESIAN_POINT('Ctrl Pts',(-20.4094530964339,24.2724036806654,15.4776605649694));
#48074=CARTESIAN_POINT('Ctrl Pts',(-20.4089137614743,24.2700539663231,15.4775112182819));
#48075=CARTESIAN_POINT('Ctrl Pts',(-20.407314195797,24.26304911804,15.4770665606779));
#48076=CARTESIAN_POINT('Ctrl Pts',(-20.4062616663822,24.25839220456,15.4767716926295));
#48077=CARTESIAN_POINT('Ctrl Pts',(-20.3966254484465,24.2153117949452,15.4740506624236));
#48078=CARTESIAN_POINT('Ctrl Pts',(-20.3887357134796,24.1767342596741,15.4716636547151));
#48079=CARTESIAN_POINT('Ctrl Pts',(-20.381075756434,24.1354388437405,15.4691518318476));
#48080=CARTESIAN_POINT('Ctrl Pts',(-20.3806001753773,24.1328573658998,15.4689949916503));
#48081=CARTESIAN_POINT('Ctrl Pts',(-20.3798508359552,24.1287618379348,15.4687464452301));
#48082=CARTESIAN_POINT('Ctrl Pts',(-20.3795750080064,24.1272481734025,15.4686546459898));
#48083=CARTESIAN_POINT('Ctrl Pts',(-20.378758431994,24.1227487719266,15.4683819502308));
#48084=CARTESIAN_POINT('Ctrl Pts',(-20.3782208150995,24.119762460111,15.4682011933681));
#48085=CARTESIAN_POINT('Ctrl Pts',(-20.3774773245037,24.115598864017,15.4679494990604));
#48086=CARTESIAN_POINT('Ctrl Pts',(-20.3772678885358,24.114422227019,15.4678784057643));
#48087=CARTESIAN_POINT('Ctrl Pts',(-20.3297356349389,23.8465164972107,15.4516994338179));
#48088=CARTESIAN_POINT('Ctrl Pts',(-20.3162247375172,23.5748522487775,15.4370448082681));
#48089=CARTESIAN_POINT('Ctrl Pts',(-20.3474176136987,23.1666976550411,15.4139365461235));
#48090=CARTESIAN_POINT('Ctrl Pts',(-20.3668364614817,23.0295587740683,15.4059975116656));
#48091=CARTESIAN_POINT('Ctrl Pts',(-20.4065382737658,22.8386439934997,15.3944206003304));
#48092=CARTESIAN_POINT('Ctrl Pts',(-20.4195303497392,22.7835035150612,15.3910149770569));
#48093=CARTESIAN_POINT('Ctrl Pts',(-20.4360526038835,22.7208290905679,15.3870633792164));
#48094=CARTESIAN_POINT('Ctrl Pts',(-20.4381672332837,22.712929697573,15.3865638517416));
#48095=CARTESIAN_POINT('Ctrl Pts',(-20.441406838606,22.70100966333,15.3858078168937));
#48096=CARTESIAN_POINT('Ctrl Pts',(-20.4425096109953,22.6969829778683,15.3855520322035));
#48097=CARTESIAN_POINT('Ctrl Pts',(-20.4444270450495,22.6900346472625,15.3851099799567));
#48098=CARTESIAN_POINT('Ctrl Pts',(-20.445238014418,22.6871119813837,15.384923832905));
#48099=CARTESIAN_POINT('Ctrl Pts',(-20.4469236432282,22.6810702342247,15.3845385982831));
#48100=CARTESIAN_POINT('Ctrl Pts',(-20.4477988816613,22.6779513190964,15.3843394920006));
#48101=CARTESIAN_POINT('Ctrl Pts',(-20.4501846206382,22.6694987414862,15.3837992463022));
#48102=CARTESIAN_POINT('Ctrl Pts',(-20.4517041776177,22.6641676661421,15.3834578115614));
#48103=CARTESIAN_POINT('Ctrl Pts',(-20.4574252399326,22.6442910919145,15.3821821631118));
#48104=CARTESIAN_POINT('Ctrl Pts',(-20.4617154229795,22.6297715147562,15.3812450539191));
#48105=CARTESIAN_POINT('Ctrl Pts',(-20.5370512472136,22.3812644125251,15.3651140999572));
#48106=CARTESIAN_POINT('Ctrl Pts',(-20.6343829522037,22.1561320254541,15.3490034052628));
#48107=CARTESIAN_POINT('Ctrl Pts',(-20.8482050969422,21.7841426536676,15.3200419270049));
#48108=CARTESIAN_POINT('Ctrl Pts',(-20.9538001837811,21.6322731764394,15.3074377923054));
#48109=CARTESIAN_POINT('Ctrl Pts',(-21.1145341836154,21.4388883218212,15.2909334923109));
#48110=CARTESIAN_POINT('Ctrl Pts',(-21.1588381554949,21.3888359843137,15.2866178325179));
#48111=CARTESIAN_POINT('Ctrl Pts',(-21.2095996763094,21.3349617050405,15.281956982503));
#48112=CARTESIAN_POINT('Ctrl Pts',(-21.2145468206594,21.3297462673864,15.2815056114234));
#48113=CARTESIAN_POINT('Ctrl Pts',(-21.2221121193208,21.3218239455839,15.2808197809941));
#48114=CARTESIAN_POINT('Ctrl Pts',(-21.2247175965876,21.3191050670341,15.280584374788));
#48115=CARTESIAN_POINT('Ctrl Pts',(-21.2295406169146,21.3140897554197,15.280150085343));
#48116=CARTESIAN_POINT('Ctrl Pts',(-21.2317568139424,21.3117920427927,15.2799510994259));
#48117=CARTESIAN_POINT('Ctrl Pts',(-21.235373233458,21.3080537374451,15.2796273276305));
#48118=CARTESIAN_POINT('Ctrl Pts',(-21.2367713884605,21.3066111614458,15.279502380391));
#48119=CARTESIAN_POINT('Ctrl Pts',(-21.2394851735825,21.3038163900534,15.2792603026163));
#48120=CARTESIAN_POINT('Ctrl Pts',(-21.2408006384053,21.3024640464529,15.2791431601776));
#48121=CARTESIAN_POINT('Ctrl Pts',(-21.243828909392,21.299356343073,15.2788739520684));
#48122=CARTESIAN_POINT('Ctrl Pts',(-21.245542536554,21.2976017785014,15.2787219511919));
#48123=CARTESIAN_POINT('Ctrl Pts',(-21.2509897641034,21.2920371424173,15.2782398393461));
#48124=CARTESIAN_POINT('Ctrl Pts',(-21.2547308471595,21.2882343585588,15.2779103149811));
#48125=CARTESIAN_POINT('Ctrl Pts',(-21.286752279709,21.2558460556432,15.2751030837406));
#48126=CARTESIAN_POINT('Ctrl Pts',(-21.3155574730846,21.2277812556397,15.2726660967448));
#48127=CARTESIAN_POINT('Ctrl Pts',(-21.3479003953225,21.1974287464245,15.2700150887176));
#48128=CARTESIAN_POINT('Ctrl Pts',(-21.3509242650302,21.1946019054524,15.2697680400688));
#48129=CARTESIAN_POINT('Ctrl Pts',(-21.3597166360948,21.1864141134559,15.2690520098054));
#48130=CARTESIAN_POINT('Ctrl Pts',(-21.3654993893466,21.1810684344248,15.2685839412356));
#48131=CARTESIAN_POINT('Ctrl Pts',(-21.3748115487557,21.1725231979923,15.2678346662354));
#48132=CARTESIAN_POINT('Ctrl Pts',(-21.3783285209827,21.1693102084157,15.2675526995875));
#48133=CARTESIAN_POINT('Ctrl Pts',(-21.4571777339989,21.0975962625136,15.2612534538216));
#48134=CARTESIAN_POINT('Ctrl Pts',(-21.535713426737,21.03269015361,15.2554335131454));
#48135=CARTESIAN_POINT('Ctrl Pts',(-21.8046641279156,20.8310738832475,15.2364644558426));
#48136=CARTESIAN_POINT('Ctrl Pts',(-22.0068898575021,20.7114072452864,15.2236349585423));
#48137=CARTESIAN_POINT('Ctrl Pts',(-22.3170757046627,20.5708767963287,15.2039547327801));
#48138=CARTESIAN_POINT('Ctrl Pts',(-22.415948620411,20.5318496587097,15.1976912195881));
#48139=CARTESIAN_POINT('Ctrl Pts',(-22.5340659137831,20.491850353538,15.190139466232));
#48140=CARTESIAN_POINT('Ctrl Pts',(-22.5516212438534,20.4860732525825,15.1890154211229));
#48141=CARTESIAN_POINT('Ctrl Pts',(-22.5747324976437,20.4786875143426,15.1875331560615));
#48142=CARTESIAN_POINT('Ctrl Pts',(-22.5802446808093,20.4769423030995,15.1871794420625));
#48143=CARTESIAN_POINT('Ctrl Pts',(-22.589246227679,20.4741189546077,15.1866015063355));
#48144=CARTESIAN_POINT('Ctrl Pts',(-22.592732796947,20.4730318932233,15.1863775784982));
#48145=CARTESIAN_POINT('Ctrl Pts',(-22.5994530946534,20.4709491297104,15.1859458123878));
#48146=CARTESIAN_POINT('Ctrl Pts',(-22.6026865597278,20.4699525885753,15.1857380020118));
#48147=CARTESIAN_POINT('Ctrl Pts',(-22.6100998746796,20.4676806117007,15.185261403286));
#48148=CARTESIAN_POINT('Ctrl Pts',(-22.6142807547415,20.4664085841392,15.1849925034942));
#48149=CARTESIAN_POINT('Ctrl Pts',(-22.6274548874138,20.4624296293219,15.1841448255665));
#48150=CARTESIAN_POINT('Ctrl Pts',(-22.6364573317819,20.4597535269498,15.1835650388066));
#48151=CARTESIAN_POINT('Ctrl Pts',(-22.6709944866181,20.4496509728991,15.1813386074721));
#48152=CARTESIAN_POINT('Ctrl Pts',(-22.696608492334,20.4425014924525,15.1796829506453));
#48153=CARTESIAN_POINT('Ctrl Pts',(-22.7282753936962,20.4340835246519,15.1776300585123));
#48154=CARTESIAN_POINT('Ctrl Pts',(-22.7342478640688,20.4325142364873,15.1772426167023));
#48155=CARTESIAN_POINT('Ctrl Pts',(-22.7464339164629,20.4293497216696,15.1764515533295));
#48156=CARTESIAN_POINT('Ctrl Pts',(-22.7526478224724,20.4277558635325,15.1760478898224));
#48157=CARTESIAN_POINT('Ctrl Pts',(-22.7613901763673,20.4255412610371,15.1754795693248));
#48158=CARTESIAN_POINT('Ctrl Pts',(-22.7639147105546,20.4249050035615,15.1753154076237));
#48159=CARTESIAN_POINT('Ctrl Pts',(-22.7687362413967,20.4236960465668,15.1750017891014));
#48160=CARTESIAN_POINT('Ctrl Pts',(-22.7710331045438,20.4231228172442,15.1748523492251));
#48161=CARTESIAN_POINT('Ctrl Pts',(-22.7800332404975,20.4208871801433,15.174266621919));
#48162=CARTESIAN_POINT('Ctrl Pts',(-22.7867411811505,20.4192438002433,15.1738297333345));
#48163=CARTESIAN_POINT('Ctrl Pts',(-22.796355025571,20.4169212344985,15.1732030956015));
#48164=CARTESIAN_POINT('Ctrl Pts',(-22.7992567043272,20.4162244949806,15.1730138984676));
#48165=CARTESIAN_POINT('Ctrl Pts',(-22.8152918662345,20.4123977440666,15.1719680114225));
#48166=CARTESIAN_POINT('Ctrl Pts',(-22.8284437973141,20.4093462946019,15.1711088770574));
#48167=CARTESIAN_POINT('Ctrl Pts',(-22.8482596462374,20.4048797469945,15.1698124439125));
#48168=CARTESIAN_POINT('Ctrl Pts',(-22.8549096267377,20.4034029627802,15.1693770398057));
#48169=CARTESIAN_POINT('Ctrl Pts',(-22.9014346059578,20.3932256744313,15.1663284886484));
#48170=CARTESIAN_POINT('Ctrl Pts',(-22.9414656349688,20.3852625534951,15.1636933154414));
#48171=CARTESIAN_POINT('Ctrl Pts',(-23.2280657283857,20.3338893385865,15.1447425769996));
#48172=CARTESIAN_POINT('Ctrl Pts',(-23.4787839086086,20.3185875864077,15.1276255812372));
#48173=CARTESIAN_POINT('Ctrl Pts',(-23.8095791909902,20.33693192408,15.1053478194706));
#48174=CARTESIAN_POINT('Ctrl Pts',(-23.8902688800614,20.3444655574046,15.099947095778));
#48175=CARTESIAN_POINT('Ctrl Pts',(-24.0288655956852,20.3626983723381,15.0908130985448));
#48176=CARTESIAN_POINT('Ctrl Pts',(-24.0869218621184,20.3719575365073,15.0870309107458));
#48177=CARTESIAN_POINT('Ctrl Pts',(-24.1512493766936,20.3840300495933,15.0829129643838));
#48178=CARTESIAN_POINT('Ctrl Pts',(-24.15779839923,20.3852801724858,15.0824945734581));
#48179=CARTESIAN_POINT('Ctrl Pts',(-24.1678442907904,20.3872301324019,15.0818541316317));
#48180=CARTESIAN_POINT('Ctrl Pts',(-24.1713439083479,20.3879154558174,15.0816312771457));
#48181=CARTESIAN_POINT('Ctrl Pts',(-24.1771085166777,20.389054266434,15.0812646119984));
#48182=CARTESIAN_POINT('Ctrl Pts',(-24.1793741589154,20.3895043803166,15.081120610776));
#48183=CARTESIAN_POINT('Ctrl Pts',(-24.1836712371576,20.3903628817954,15.0808477012696));
#48184=CARTESIAN_POINT('Ctrl Pts',(-24.1857027653732,20.3907707930948,15.080718765799));
#48185=CARTESIAN_POINT('Ctrl Pts',(-24.1895245948165,20.3915420148926,15.0804763720654));
#48186=CARTESIAN_POINT('Ctrl Pts',(-24.1913149733679,20.3919048868709,15.0803628892832));
#48187=CARTESIAN_POINT('Ctrl Pts',(-24.1952621540202,20.3927083917828,15.0801128506953));
#48188=CARTESIAN_POINT('Ctrl Pts',(-24.1974188080795,20.3931497112017,15.0799763352771));
#48189=CARTESIAN_POINT('Ctrl Pts',(-24.2033660651773,20.3943730575938,15.0796001484074));
#48190=CARTESIAN_POINT('Ctrl Pts',(-24.2071557300403,20.395159707221,15.0793607428334));
#48191=CARTESIAN_POINT('Ctrl Pts',(-24.2266051021672,20.3992335228834,15.0781335872822));
#48192=CARTESIAN_POINT('Ctrl Pts',(-24.2422419464662,20.402630529567,15.0771520616261));
#48193=CARTESIAN_POINT('Ctrl Pts',(-24.5721978193018,20.4768890979609,15.0565357612891));
#48194=CARTESIAN_POINT('Ctrl Pts',(-24.8742152495325,20.5943871070597,15.0393528562809));
#48195=CARTESIAN_POINT('Ctrl Pts',(-25.2067127340257,20.7851167331773,15.0176191495377));
#48196=CARTESIAN_POINT('Ctrl Pts',(-25.258736136087,20.8169542181277,15.0141329978844));
#48197=CARTESIAN_POINT('Ctrl Pts',(-25.3754724415382,20.8930302925773,15.0060696039607));
#48198=CARTESIAN_POINT('Ctrl Pts',(-25.4395350599354,20.9381905379804,15.0014669953377));
#48199=CARTESIAN_POINT('Ctrl Pts',(-25.5335331491884,21.0097216449567,14.9943957490371));
#48200=CARTESIAN_POINT('Ctrl Pts',(-25.5647316292989,21.0343882779344,14.9919931208424));
#48201=CARTESIAN_POINT('Ctrl Pts',(-25.6012263442089,21.0643564024758,14.9891124669186));
#48202=CARTESIAN_POINT('Ctrl Pts',(-25.6069715717371,21.0691076480295,14.9886568704943));
#48203=CARTESIAN_POINT('Ctrl Pts',(-25.6157910922121,21.0764529849152,14.9879542094789));
#48204=CARTESIAN_POINT('Ctrl Pts',(-25.6188771277236,21.079032990031,14.9877077208925));
#48205=CARTESIAN_POINT('Ctrl Pts',(-25.6242685097912,21.0835574997075,14.9872760075908));
#48206=CARTESIAN_POINT('Ctrl Pts',(-25.6265759769405,21.0854994793879,14.987090886624));
#48207=CARTESIAN_POINT('Ctrl Pts',(-25.6317826722372,21.0898939690308,14.9866723731695));
#48208=CARTESIAN_POINT('Ctrl Pts',(-25.6346802946091,21.0923483667901,14.9864389031429));
#48209=CARTESIAN_POINT('Ctrl Pts',(-25.6424738086489,21.0989734665222,14.985809442644));
#48210=CARTESIAN_POINT('Ctrl Pts',(-25.6473615455672,21.103153696325,14.9854130590041));
#48211=CARTESIAN_POINT('Ctrl Pts',(-25.668846112426,21.1216399811268,14.983663544704));
#48212=CARTESIAN_POINT('Ctrl Pts',(-25.6853089910335,21.1361001839078,14.9823040190447));
#48213=CARTESIAN_POINT('Ctrl Pts',(-25.7111635530089,21.1592809053668,14.9801382370392));
#48214=CARTESIAN_POINT('Ctrl Pts',(-25.7206530754617,21.1678916791159,14.9793366398407));
#48215=CARTESIAN_POINT('Ctrl Pts',(-25.7397729568686,21.1854500729292,14.977707862806));
#48216=CARTESIAN_POINT('Ctrl Pts',(-25.7494004213254,21.1944004751071,14.9768805733507));
#48217=CARTESIAN_POINT('Ctrl Pts',(-25.7639915476151,21.2081328441055,14.9756157463722));
#48218=CARTESIAN_POINT('Ctrl Pts',(-25.7689951542247,21.212872323986,14.9751800136716));
#48219=CARTESIAN_POINT('Ctrl Pts',(-25.7781859878633,21.221634102467,14.9743759447204));
#48220=CARTESIAN_POINT('Ctrl Pts',(-25.7823776306145,21.2256517452964,14.9740078063447));
#48221=CARTESIAN_POINT('Ctrl Pts',(-25.7894741752755,21.2324905959042,14.9733821057411));
#48222=CARTESIAN_POINT('Ctrl Pts',(-25.7923846697175,21.2353060019694,14.9731247888244));
#48223=CARTESIAN_POINT('Ctrl Pts',(-25.8006006557055,21.2432835939391,14.9723964303817));
#48224=CARTESIAN_POINT('Ctrl Pts',(-25.8058936536369,21.2484585603392,14.9719248514698));
#48225=CARTESIAN_POINT('Ctrl Pts',(-25.821346241917,21.2636710459271,14.9705411987586));
#48226=CARTESIAN_POINT('Ctrl Pts',(-25.8314568986725,21.2737578232613,14.9696270653708));
#48227=CARTESIAN_POINT('Ctrl Pts',(-26.021187952798,21.4655739584263,14.9523053259293));
#48228=CARTESIAN_POINT('Ctrl Pts',(-26.1786091851035,21.6679383275251,14.9349653653267));
#48229=CARTESIAN_POINT('Ctrl Pts',(-26.4003916535136,22.035928612022,14.9059419247136));
#48230=CARTESIAN_POINT('Ctrl Pts',(-26.4780870094096,22.1922125929812,14.8942909339694));
#48231=CARTESIAN_POINT('Ctrl Pts',(-26.5449144499306,22.3593911336872,14.8830143385004));
#48232=CARTESIAN_POINT('Ctrl Pts',(-26.5470423699649,22.3647562051429,14.8826536831015));
#48233=CARTESIAN_POINT('Ctrl Pts',(-26.5500935487412,22.3725097789139,14.8821342722929));
#48234=CARTESIAN_POINT('Ctrl Pts',(-26.5510283760272,22.3748936709793,14.8819748217399));
#48235=CARTESIAN_POINT('Ctrl Pts',(-26.5526507982834,22.3790455432546,14.8816975482373));
#48236=CARTESIAN_POINT('Ctrl Pts',(-26.5533396742809,22.3808130184685,14.8815796473175));
#48237=CARTESIAN_POINT('Ctrl Pts',(-26.554671169337,22.3842382207799,14.8813514307984));
#48238=CARTESIAN_POINT('Ctrl Pts',(-26.555313975532,22.3858958671492,14.8812411038011));
#48239=CARTESIAN_POINT('Ctrl Pts',(-26.5568465695567,22.3898577905069,14.8809776963718));
#48240=CARTESIAN_POINT('Ctrl Pts',(-26.5577350821936,22.3921625643677,14.8808246934279));
#48241=CARTESIAN_POINT('Ctrl Pts',(-26.5609044796981,22.4004121282887,14.8802778566236));
#48242=CARTESIAN_POINT('Ctrl Pts',(-26.5631704147708,22.4063627044817,14.8798849204014));
#48243=CARTESIAN_POINT('Ctrl Pts',(-26.59619239229,22.4938606438487,14.8741287226286));
#48244=CARTESIAN_POINT('Ctrl Pts',(-26.6236489896969,22.5766248486479,14.8689586974522));
#48245=CARTESIAN_POINT('Ctrl Pts',(-26.7306457119797,22.9490708094409,14.8464773058849));
#48246=CARTESIAN_POINT('Ctrl Pts',(-26.7728204513682,23.2479183136171,14.8303697289785));
#48247=CARTESIAN_POINT('Ctrl Pts',(-26.7730746935473,23.6687138283204,14.8060891589639));
#48248=CARTESIAN_POINT('Ctrl Pts',(-26.7663994938228,23.7890186458402,14.7989850392452));
#48249=CARTESIAN_POINT('Ctrl Pts',(-26.7518235465049,23.9192710030495,14.7910102352784));
#48250=CARTESIAN_POINT('Ctrl Pts',(-26.7505832380056,23.9298772951235,14.7903588398648));
#48251=CARTESIAN_POINT('Ctrl Pts',(-26.7487690530033,23.9447498744277,14.7894425339449));
#48252=CARTESIAN_POINT('Ctrl Pts',(-26.7482392976755,23.9490215561017,14.7891790187043));
#48253=CARTESIAN_POINT('Ctrl Pts',(-26.7473057811145,23.9564274561047,14.7887215711402));
#48254=CARTESIAN_POINT('Ctrl Pts',(-26.7469059639392,23.9595621734787,14.7885277637925));
#48255=CARTESIAN_POINT('Ctrl Pts',(-26.7460650919268,23.9660785439754,14.7881245011069));
#48256=CARTESIAN_POINT('Ctrl Pts',(-26.7456232790022,23.9694600933374,14.7879150220258));
#48257=CARTESIAN_POINT('Ctrl Pts',(-26.7445714125592,23.9774125902452,14.7874218784325));
#48258=CARTESIAN_POINT('Ctrl Pts',(-26.743956915046,23.9819829333084,14.7871380734877));
#48259=CARTESIAN_POINT('Ctrl Pts',(-26.7419206902413,23.9968851518233,14.7862113986722));
#48260=CARTESIAN_POINT('Ctrl Pts',(-26.7404586300804,24.007211367217,14.7855672518012));
#48261=CARTESIAN_POINT('Ctrl Pts',(-26.7148741631729,24.1817992818398,14.7746416895627));
#48262=CARTESIAN_POINT('Ctrl Pts',(-26.6781486131203,24.3439348442341,14.7639534537309));
#48263=CARTESIAN_POINT('Ctrl Pts',(-26.5363159612377,24.8025153798054,14.7321443059383));
#48264=CARTESIAN_POINT('Ctrl Pts',(-26.4001845830794,25.0873305771487,14.7102438007793));
#48265=CARTESIAN_POINT('Ctrl Pts',(-26.22258375519,25.3515805210341,14.6898606971357));
#48266=CARTESIAN_POINT('Ctrl Pts',(-26.2201365424214,25.3552057341273,14.6895810883095));
#48267=CARTESIAN_POINT('Ctrl Pts',(-26.2148344300244,25.3630257154467,14.6889780136434));
#48268=CARTESIAN_POINT('Ctrl Pts',(-26.2119769821574,25.3672187557089,14.688654692631));
#48269=CARTESIAN_POINT('Ctrl Pts',(-26.2044127535385,25.3782624231628,14.6878032824879));
#48270=CARTESIAN_POINT('Ctrl Pts',(-26.1996893164462,25.385101673575,14.6872761699066));
#48271=CARTESIAN_POINT('Ctrl Pts',(-26.1929507757418,25.3947783957977,14.686530681577));
#48272=CARTESIAN_POINT('Ctrl Pts',(-26.1909575010093,25.3976309276183,14.6863109631802));
#48273=CARTESIAN_POINT('Ctrl Pts',(-26.1820148240199,25.4103845497096,14.6853288000661));
#48274=CARTESIAN_POINT('Ctrl Pts',(-26.1750142084187,25.420249868379,14.6845695912735));
#48275=CARTESIAN_POINT('Ctrl Pts',(-26.1658764468832,25.4329744529136,14.6835912724674));
#48276=CARTESIAN_POINT('Ctrl Pts',(-26.1637899875912,25.4358697423885,14.6833687334791));
#48277=CARTESIAN_POINT('Ctrl Pts',(-26.1605853363612,25.4403011610429,14.6830282279546));
#48278=CARTESIAN_POINT('Ctrl Pts',(-26.1594705967788,25.4418397650258,14.682910022527));
#48279=CARTESIAN_POINT('Ctrl Pts',(-26.1572700682458,25.4448713679166,14.6826771548605));
#48280=CARTESIAN_POINT('Ctrl Pts',(-26.1561843627513,25.4463644119311,14.6825624882517));
#48281=CARTESIAN_POINT('Ctrl Pts',(-26.1537636492315,25.4496873302519,14.6823073284527));
#48282=CARTESIAN_POINT('Ctrl Pts',(-26.1524279978497,25.4515167259942,14.6821668813201));
#48283=CARTESIAN_POINT('Ctrl Pts',(-26.1485667810561,25.4567936111478,14.6817618388978));
#48284=CARTESIAN_POINT('Ctrl Pts',(-26.1460362731586,25.4602375039206,14.6814975878347));
#48285=CARTESIAN_POINT('Ctrl Pts',(-26.1289663780756,25.4833721813923,14.6797230191025));
#48286=CARTESIAN_POINT('Ctrl Pts',(-26.114209409169,25.5029025000609,14.6782276751155));
#48287=CARTESIAN_POINT('Ctrl Pts',(-26.0678641562336,25.5628073616852,14.6736430843277));
#48288=CARTESIAN_POINT('Ctrl Pts',(-26.0355326940446,25.6025995750588,14.6706006282148));
#48289=CARTESIAN_POINT('Ctrl Pts',(-25.9738659284887,25.674900894138,14.6650423979662));
#48290=CARTESIAN_POINT('Ctrl Pts',(-25.9447918384842,25.7076153544093,14.6625153370804));
#48291=CARTESIAN_POINT('Ctrl Pts',(-25.7266577909439,25.9432173336073,14.6441403618332));
#48292=CARTESIAN_POINT('Ctrl Pts',(-25.5127817460327,26.1215386636725,14.6291461523431));
#48293=CARTESIAN_POINT('Ctrl Pts',(-25.2394437272199,26.2952324533477,14.6104162374911));
#48294=CARTESIAN_POINT('Ctrl Pts',(-25.199646256108,26.3193285011329,14.6077019971461));
#48295=CARTESIAN_POINT('Ctrl Pts',(-25.0987396996147,26.3774768511741,14.600835127832));
#48296=CARTESIAN_POINT('Ctrl Pts',(-25.0370200002191,26.4104153292194,14.5966480978013));
#48297=CARTESIAN_POINT('Ctrl Pts',(-24.9657798505873,26.4455055041975,14.5918112549094));
#48298=CARTESIAN_POINT('Ctrl Pts',(-24.9572603716994,26.4496552806181,14.5912327740642));
#48299=CARTESIAN_POINT('Ctrl Pts',(-24.9447710975515,26.4556707064909,14.590384620798));
#48300=CARTESIAN_POINT('Ctrl Pts',(-24.9408155442015,26.4575659494228,14.5901159796346));
#48301=CARTESIAN_POINT('Ctrl Pts',(-24.933799537708,26.4609099677348,14.5896394521692));
#48302=CARTESIAN_POINT('Ctrl Pts',(-24.9307406410762,26.4623620089536,14.589431679746));
#48303=CARTESIAN_POINT('Ctrl Pts',(-24.9244505869723,26.4653357248933,14.5890044070043));
#48304=CARTESIAN_POINT('Ctrl Pts',(-24.9212191780416,26.4668568539912,14.5887848881121));
#48305=CARTESIAN_POINT('Ctrl Pts',(-24.9129531422857,26.4707311728466,14.5882233112979));
#48306=CARTESIAN_POINT('Ctrl Pts',(-24.9079149600735,26.473076710033,14.5878809888923));
#48307=CARTESIAN_POINT('Ctrl Pts',(-24.8969792678059,26.4781334705525,14.5871378609764));
#48308=CARTESIAN_POINT('Ctrl Pts',(-24.8910795924051,26.4808399277914,14.5867368922793));
#48309=CARTESIAN_POINT('Ctrl Pts',(-24.8741073791122,26.4885638974564,14.5855831897731));
#48310=CARTESIAN_POINT('Ctrl Pts',(-24.8630146653146,26.4935365671223,14.5848289150427));
#48311=CARTESIAN_POINT('Ctrl Pts',(-24.7558195960524,26.5408637036697,14.5775372361526));
#48312=CARTESIAN_POINT('Ctrl Pts',(-24.6577391949683,26.578555078469,14.5708414810364));
#48313=CARTESIAN_POINT('Ctrl Pts',(-24.4138606428955,26.6588418025909,14.5541183607413));
#48314=CARTESIAN_POINT('Ctrl Pts',(-24.266560986747,26.6960497299008,14.5439486847148));
#48315=CARTESIAN_POINT('Ctrl Pts',(-24.0204731939521,26.7400276904012,14.5270472441828));
#48316=CARTESIAN_POINT('Ctrl Pts',(-23.9230026808738,26.7528812531071,14.520378739078));
#48317=CARTESIAN_POINT('Ctrl Pts',(-23.6862757574035,26.773143725189,14.5044083485026));
#48318=CARTESIAN_POINT('Ctrl Pts',(-23.546810865969,26.7760126658359,14.4951842719377));
#48319=CARTESIAN_POINT('Ctrl Pts',(-23.3987828236384,26.769453064222,14.4858712199841));
#48320=CARTESIAN_POINT('Ctrl Pts',(-23.3899851006605,26.7690270649527,14.4853195366102));
#48321=CARTESIAN_POINT('Ctrl Pts',(-23.3780509692405,26.7684001447648,14.4845737445212));
#48322=CARTESIAN_POINT('Ctrl Pts',(-23.3749130521061,26.7682307020245,14.4843778895986));
#48323=CARTESIAN_POINT('Ctrl Pts',(-23.3699639664627,26.7679561984464,14.4840693749785));
#48324=CARTESIAN_POINT('Ctrl Pts',(-23.3681526407713,26.7678541980832,14.4839565425485));
#48325=CARTESIAN_POINT('Ctrl Pts',(-23.3646523099774,26.7676541203267,14.4837386560546));
#48326=CARTESIAN_POINT('Ctrl Pts',(-23.3629633073733,26.7675562430807,14.4836335916236));
#48327=CARTESIAN_POINT('Ctrl Pts',(-23.3589305565579,26.7673193598391,14.4833829042141));
#48328=CARTESIAN_POINT('Ctrl Pts',(-23.3565868843069,26.7671791227166,14.4832373516964));
#48329=CARTESIAN_POINT('Ctrl Pts',(-23.3495821336134,26.7667523003123,14.4828027290414));
#48330=CARTESIAN_POINT('Ctrl Pts',(-23.3449214968207,26.7664581434292,14.482514085542));
#48331=CARTESIAN_POINT('Ctrl Pts',(-23.3054715549848,26.7638821518488,14.480075263434));
#48332=CARTESIAN_POINT('Ctrl Pts',(-23.2707190373552,26.7610459430922,14.4779558080514));
#48333=CARTESIAN_POINT('Ctrl Pts',(-23.1436171339345,26.7485935121687,14.4702881311803));
#48334=CARTESIAN_POINT('Ctrl Pts',(-23.0516424465499,26.7355513264308,14.4649017173756));
#48335=CARTESIAN_POINT('Ctrl Pts',(-22.7437021425551,26.6782164514784,14.4470392497461));
#48336=CARTESIAN_POINT('Ctrl Pts',(-22.5317583046197,26.6157635702548,14.4349958628012));
#48337=CARTESIAN_POINT('Ctrl Pts',(-22.2418952315318,26.4969365178865,14.4171747671787));
#48338=CARTESIAN_POINT('Ctrl Pts',(-22.1575504760193,26.4580200681639,14.4118201147606));
#48339=CARTESIAN_POINT('Ctrl Pts',(-22.0750358569346,26.4155366929967,14.4063516850465));
#48340=CARTESIAN_POINT('',(-26.773001504593,23.5528255026527,14.5642265507266));
#48341=CARTESIAN_POINT('Ctrl Pts',(-22.0750361586249,26.4155368483246,14.1564144975666));
#48342=CARTESIAN_POINT('Ctrl Pts',(-22.1641783660915,26.4614324836105,14.1620444840364));
#48343=CARTESIAN_POINT('Ctrl Pts',(-22.2554435166684,26.5031584476492,14.1677232490408));
#48344=CARTESIAN_POINT('Ctrl Pts',(-22.4570048561852,26.584159622923,14.180274845889));
#48345=CARTESIAN_POINT('Ctrl Pts',(-22.5677517397116,26.6218107828571,14.1871789315501));
#48346=CARTESIAN_POINT('Ctrl Pts',(-22.6905015721636,26.6562239284404,14.1949361318805));
#48347=CARTESIAN_POINT('Ctrl Pts',(-22.7007269020646,26.6590362536987,14.1955830634446));
#48348=CARTESIAN_POINT('Ctrl Pts',(-22.7151095437004,26.6629157276887,14.1964941156984));
#48349=CARTESIAN_POINT('Ctrl Pts',(-22.7192554682639,26.6640251409857,14.1967568624061));
#48350=CARTESIAN_POINT('Ctrl Pts',(-22.7264549100795,26.6659362460338,14.197213351087));
#48351=CARTESIAN_POINT('Ctrl Pts',(-22.7295074197282,26.6667417407651,14.1974069693806));
#48352=CARTESIAN_POINT('Ctrl Pts',(-22.7356519942143,26.668353514313,14.1977968587649));
#48353=CARTESIAN_POINT('Ctrl Pts',(-22.73874408382,26.6691596820251,14.1979931331792));
#48354=CARTESIAN_POINT('Ctrl Pts',(-22.7450506789853,26.6707939202462,14.1983936038051));
#48355=CARTESIAN_POINT('Ctrl Pts',(-22.748265274243,26.6716216255416,14.1985978115815));
#48356=CARTESIAN_POINT('Ctrl Pts',(-22.7588562884303,26.6743311961511,14.1992708749277));
#48357=CARTESIAN_POINT('Ctrl Pts',(-22.7662380549854,26.6761918807994,14.1997404158028));
#48358=CARTESIAN_POINT('Ctrl Pts',(-22.815689199483,26.6884705998276,14.2028888506412));
#48359=CARTESIAN_POINT('Ctrl Pts',(-22.8579567457468,26.69806481661,14.2055942225938));
#48360=CARTESIAN_POINT('Ctrl Pts',(-22.9788744967297,26.7229585406235,14.2133789343628));
#48361=CARTESIAN_POINT('Ctrl Pts',(-23.0579147690575,26.7361806566581,14.2185224199575));
#48362=CARTESIAN_POINT('Ctrl Pts',(-23.238766482207,26.7595435463649,14.2304158806061));
#48363=CARTESIAN_POINT('Ctrl Pts',(-23.3407311575276,26.7678091130739,14.2372112876052));
#48364=CARTESIAN_POINT('Ctrl Pts',(-23.696661026257,26.779670976963,14.2611378849326));
#48365=CARTESIAN_POINT('Ctrl Pts',(-23.9505269205996,26.7581130096931,14.2786384522413));
#48366=CARTESIAN_POINT('Ctrl Pts',(-24.2336370473986,26.6999091137219,14.2971958614323));
#48367=CARTESIAN_POINT('Ctrl Pts',(-24.2679215223982,26.6922745642199,14.2994251894649));
#48368=CARTESIAN_POINT('Ctrl Pts',(-24.3065681413952,26.6830030167128,14.301912505102));
#48369=CARTESIAN_POINT('Ctrl Pts',(-24.3110579527206,26.6819156704801,14.3022010775983));
#48370=CARTESIAN_POINT('Ctrl Pts',(-24.3178488723063,26.6802555737431,14.3026369357577));
#48371=CARTESIAN_POINT('Ctrl Pts',(-24.3201516878883,26.6796899371613,14.3027846294433));
#48372=CARTESIAN_POINT('Ctrl Pts',(-24.3241551349439,26.6787018909967,14.3030412068006));
#48373=CARTESIAN_POINT('Ctrl Pts',(-24.3258560459269,26.6782806360725,14.3031501575395));
#48374=CARTESIAN_POINT('Ctrl Pts',(-24.329415931752,26.6773958973065,14.3033780586469));
#48375=CARTESIAN_POINT('Ctrl Pts',(-24.3312748358626,26.6769321432784,14.3034969926689));
#48376=CARTESIAN_POINT('Ctrl Pts',(-24.3357203219702,26.6758188844018,14.3037812491499));
#48377=CARTESIAN_POINT('Ctrl Pts',(-24.3383065211397,26.6751678240791,14.3039464809324));
#48378=CARTESIAN_POINT('Ctrl Pts',(-24.3470718451704,26.6729496321965,14.3045060410579));
#48379=CARTESIAN_POINT('Ctrl Pts',(-24.3532471785621,26.6713673643394,14.3048994948597));
#48380=CARTESIAN_POINT('Ctrl Pts',(-24.3679138507566,26.6675630020536,14.3058322288875));
#48381=CARTESIAN_POINT('Ctrl Pts',(-24.3764009378211,26.6653245078243,14.306370584403));
#48382=CARTESIAN_POINT('Ctrl Pts',(-24.4761887867704,26.6385686608135,14.3126851866119));
#48383=CARTESIAN_POINT('Ctrl Pts',(-24.5663871581839,26.6100774708763,14.3182436659957));
#48384=CARTESIAN_POINT('Ctrl Pts',(-24.7713446553043,26.5352710073156,14.330801792821));
#48385=CARTESIAN_POINT('Ctrl Pts',(-24.8849493767254,26.486234272644,14.337710505534));
#48386=CARTESIAN_POINT('Ctrl Pts',(-25.0496056072956,26.4036237934179,14.3480044251567));
#48387=CARTESIAN_POINT('Ctrl Pts',(-25.1029736045383,26.3749373604643,14.3513867446968));
#48388=CARTESIAN_POINT('Ctrl Pts',(-25.225170614364,26.3047438565162,14.3592958519203));
#48389=CARTESIAN_POINT('Ctrl Pts',(-25.2933169115535,26.2621335740474,14.3638334831546));
#48390=CARTESIAN_POINT('Ctrl Pts',(-25.4035077904985,26.1873632202491,14.3714638067219));
#48391=CARTESIAN_POINT('Ctrl Pts',(-25.4464805492464,26.1566344622288,14.3745176501839));
#48392=CARTESIAN_POINT('Ctrl Pts',(-25.5067964734806,26.1112226155249,14.3789327435448));
#48393=CARTESIAN_POINT('Ctrl Pts',(-25.5247707707015,26.0973900732245,14.3802653389994));
#48394=CARTESIAN_POINT('Ctrl Pts',(-25.5465191581981,26.0802845501943,14.3818993738021));
#48395=CARTESIAN_POINT('Ctrl Pts',(-25.5504338636023,26.0771908170175,14.3821943647709));
#48396=CARTESIAN_POINT('Ctrl Pts',(-25.6028032791899,26.0356061095346,14.3861523487597));
#48397=CARTESIAN_POINT('Ctrl Pts',(-25.6501440365499,25.9957385478484,14.3898652816964));
#48398=CARTESIAN_POINT('Ctrl Pts',(-25.7031301873842,25.9484433175447,14.3941921800626));
#48399=CARTESIAN_POINT('Ctrl Pts',(-25.7099287763556,25.9423227148695,14.3947506942733));
#48400=CARTESIAN_POINT('Ctrl Pts',(-25.7199020269315,25.9332668671974,14.3955749814105));
#48401=CARTESIAN_POINT('Ctrl Pts',(-25.7230970300878,25.9303540087134,14.3958398045199));
#48402=CARTESIAN_POINT('Ctrl Pts',(-25.728776917582,25.9251547328287,14.3963119463658));
#48403=CARTESIAN_POINT('Ctrl Pts',(-25.7312640929222,25.9228708184216,14.3965191582762));
#48404=CARTESIAN_POINT('Ctrl Pts',(-25.736052291107,25.9184600379189,14.3969189733547));
#48405=CARTESIAN_POINT('Ctrl Pts',(-25.7383538116413,25.9163337157137,14.3971115531361));
#48406=CARTESIAN_POINT('Ctrl Pts',(-25.7432952411801,25.9117550660842,14.3975258960409));
#48407=CARTESIAN_POINT('Ctrl Pts',(-25.7459341437246,25.9093016630144,14.3977477051942));
#48408=CARTESIAN_POINT('Ctrl Pts',(-25.7560329905152,25.8998810815878,14.398598608407));
#48409=CARTESIAN_POINT('Ctrl Pts',(-25.763463871326,25.8928829586436,14.3992290341238));
#48410=CARTESIAN_POINT('Ctrl Pts',(-25.8517051950243,25.8089860180301,14.4067673991941));
#48411=CARTESIAN_POINT('Ctrl Pts',(-25.9284946006083,25.7279855359648,14.4138554609292));
#48412=CARTESIAN_POINT('Ctrl Pts',(-26.0447763978912,25.5918273828638,14.425499015566));
#48413=CARTESIAN_POINT('Ctrl Pts',(-26.0870016270923,25.5391166091991,14.4299464752438));
#48414=CARTESIAN_POINT('Ctrl Pts',(-26.3180134503841,25.2314039962296,14.4555402933867));
#48415=CARTESIAN_POINT('Ctrl Pts',(-26.4699719113487,24.9509684018659,14.4776782685235));
#48416=CARTESIAN_POINT('Ctrl Pts',(-26.5841299806454,24.6374390849412,14.498798408725));
#48417=CARTESIAN_POINT('Ctrl Pts',(-26.5896279345108,24.6219727212992,14.4998310489897));
#48418=CARTESIAN_POINT('Ctrl Pts',(-26.5961883188077,24.6030610242234,14.5010819317832));
#48419=CARTESIAN_POINT('Ctrl Pts',(-26.5973633176643,24.599655409286,14.5013067259906));
#48420=CARTESIAN_POINT('Ctrl Pts',(-26.5992889638398,24.5940436163952,14.5016763702168));
#48421=CARTESIAN_POINT('Ctrl Pts',(-26.6000429289758,24.5918385942801,14.5018214169399));
#48422=CARTESIAN_POINT('Ctrl Pts',(-26.6013967674909,24.5878651289874,14.5020824361927));
#48423=CARTESIAN_POINT('Ctrl Pts',(-26.601997494122,24.5860969862593,14.5021984595274));
#48424=CARTESIAN_POINT('Ctrl Pts',(-26.603284553985,24.582297893637,14.5024474781995));
#48425=CARTESIAN_POINT('Ctrl Pts',(-26.6039703957749,24.5802667864014,14.5025804437681));
#48426=CARTESIAN_POINT('Ctrl Pts',(-26.6058397103479,24.5747125694664,14.5029435952363));
#48427=CARTESIAN_POINT('Ctrl Pts',(-26.6070191208747,24.5711880805637,14.5031735391021));
#48428=CARTESIAN_POINT('Ctrl Pts',(-26.6130654722392,24.5530150753995,14.5043566519487));
#48429=CARTESIAN_POINT('Ctrl Pts',(-26.617833330556,24.5383334457727,14.5053040162349));
#48430=CARTESIAN_POINT('Ctrl Pts',(-26.6621301977274,24.3985187724267,14.5142507940164));
#48431=CARTESIAN_POINT('Ctrl Pts',(-26.694092175547,24.2710988209974,14.5218366642828));
#48432=CARTESIAN_POINT('Ctrl Pts',(-26.7545046808052,23.9477161584249,14.5404829065207));
#48433=CARTESIAN_POINT('Ctrl Pts',(-26.7728495125508,23.75044052546,14.55133804464));
#48434=CARTESIAN_POINT('Ctrl Pts',(-26.7730015784458,23.5527312736527,14.5625675171146));
#48435=CARTESIAN_POINT('Ctrl Pts',(-26.773001504593,23.5528255026527,14.5642265507266));
#48436=CARTESIAN_POINT('Ctrl Pts',(-26.7730811417884,23.4530767321105,14.5703666451467));
#48437=CARTESIAN_POINT('Ctrl Pts',(-26.7685254240945,23.353267963731,14.5765067395667));
#48438=CARTESIAN_POINT('Ctrl Pts',(-26.7593443695323,23.25386235166,14.5826468339868));
#48439=CARTESIAN_POINT('Ctrl Pts',(-26.7501651566195,23.1544766795947,14.5887856967508));
#48440=CARTESIAN_POINT('Ctrl Pts',(-26.7363624905339,23.0554944367485,14.5949245595149));
#48441=CARTESIAN_POINT('Ctrl Pts',(-26.7179983712085,22.9573749231272,14.6010634222789));
#48442=CARTESIAN_POINT('Ctrl Pts',(-26.6996329917632,22.8592486766843,14.607202706283));
#48443=CARTESIAN_POINT('Ctrl Pts',(-26.676705617717,22.7619857052364,14.6133419902871));
#48444=CARTESIAN_POINT('Ctrl Pts',(-26.6493294175796,22.6660353536938,14.6194812742912));
#48445=CARTESIAN_POINT('Ctrl Pts',(-26.6219439689296,22.5700525872058,14.6256226323321));
#48446=CARTESIAN_POINT('Ctrl Pts',(-26.5901068274062,22.4753837404078,14.6317639903729));
#48447=CARTESIAN_POINT('Ctrl Pts',(-26.5539807836201,22.3824622461197,14.6379053484138));
#48448=CARTESIAN_POINT('Ctrl Pts',(-26.5178109255119,22.2894280549555,14.6440541548052));
#48449=CARTESIAN_POINT('Ctrl Pts',(-26.4773419433713,22.1981458514324,14.6502029611966));
#48450=CARTESIAN_POINT('Ctrl Pts',(-26.4327843892806,22.1090281728591,14.6563517675881));
#48451=CARTESIAN_POINT('Ctrl Pts',(-26.3881946596312,22.0198461413124,14.6625050141083));
#48452=CARTESIAN_POINT('Ctrl Pts',(-26.3395106942905,21.9328321246508,14.6686582606286));
#48453=CARTESIAN_POINT('Ctrl Pts',(-26.2869874634296,21.8483713737048,14.6748115071489));
#48454=CARTESIAN_POINT('Ctrl Pts',(-26.2343808308645,21.7637765074264,14.680974524417));
#48455=CARTESIAN_POINT('Ctrl Pts',(-26.1779230150736,21.6817433535447,14.6871375416852));
#48456=CARTESIAN_POINT('Ctrl Pts',(-26.1179103271923,21.6026255120321,14.6933005589533));
#48457=CARTESIAN_POINT('Ctrl Pts',(-26.1026662866333,21.5825285020907,14.6948660493274));
#48458=CARTESIAN_POINT('Ctrl Pts',(-26.0871930643724,21.562619414593,14.6964315397015));
#48459=CARTESIAN_POINT('Ctrl Pts',(-26.0714958924752,21.5429036636054,14.6979970300756));
#48460=CARTESIAN_POINT('Ctrl Pts',(-26.0096083332172,21.4651724827555,14.7041691213879));
#48461=CARTESIAN_POINT('Ctrl Pts',(-25.9440136725124,21.3901691187462,14.7103412127002));
#48462=CARTESIAN_POINT('Ctrl Pts',(-25.8749813413925,21.3182683194161,14.7165133040125));
#48463=CARTESIAN_POINT('Ctrl Pts',(-25.8060425422565,21.2464649385607,14.7226770327513));
#48464=CARTESIAN_POINT('Ctrl Pts',(-25.7336756285893,21.1777560777395,14.7288407614901));
#48465=CARTESIAN_POINT('Ctrl Pts',(-25.6581911001744,21.1124845866236,14.7350044902289));
#48466=CARTESIAN_POINT('Ctrl Pts',(-25.5827865405327,21.0472822445265,14.7411616890756));
#48467=CARTESIAN_POINT('Ctrl Pts',(-25.5042712592279,20.9855103149272,14.7473188879223));
#48468=CARTESIAN_POINT('Ctrl Pts',(-25.4229928425718,20.9274751315868,14.7534760867689));
#48469=CARTESIAN_POINT('Ctrl Pts',(-25.3417738355096,20.8694823684463,14.7596287850766));
#48470=CARTESIAN_POINT('Ctrl Pts',(-25.2577960610316,20.8152211728802,14.7657814833844));
#48471=CARTESIAN_POINT('Ctrl Pts',(-25.1714397252606,20.7649572787782,14.7719341816921));
#48472=CARTESIAN_POINT('Ctrl Pts',(-25.0851161359348,20.7147124448163,14.7780845468878));
#48473=CARTESIAN_POINT('Ctrl Pts',(-24.9964161525077,20.668462118755,14.7842349120836));
#48474=CARTESIAN_POINT('Ctrl Pts',(-24.905747714114,20.626427917779,14.7903852772793));
#48475=CARTESIAN_POINT('Ctrl Pts',(-24.8150894008456,20.5843984108459,14.7965349556515));
#48476=CARTESIAN_POINT('Ctrl Pts',(-24.7224634637546,20.5465842756483,14.8026846340238));
#48477=CARTESIAN_POINT('Ctrl Pts',(-24.6283002022478,20.51316004339,14.808834312396));
#48478=CARTESIAN_POINT('Ctrl Pts',(-24.5341222648933,20.4797306017863,14.8149849492284));
#48479=CARTESIAN_POINT('Ctrl Pts',(-24.4384069366313,20.4506925674244,14.8211355860609));
#48480=CARTESIAN_POINT('Ctrl Pts',(-24.3416011846338,20.4261710871748,14.8272862228933));
#48481=CARTESIAN_POINT('Ctrl Pts',(-24.2446918708176,20.4016233740925,14.8334434396151));
#48482=CARTESIAN_POINT('Ctrl Pts',(-24.1466902257566,20.381601970555,14.839600656337));
#48483=CARTESIAN_POINT('Ctrl Pts',(-24.0480548466727,20.3661811729301,14.8457578730588));
#48484=CARTESIAN_POINT('Ctrl Pts',(-23.9493644393148,20.3507517721053,14.8519185248666));
#48485=CARTESIAN_POINT('Ctrl Pts',(-23.8500400256912,20.3399281357169,14.8580791766744));
#48486=CARTESIAN_POINT('Ctrl Pts',(-23.7505446914926,20.3337325778896,14.8642398284822));
#48487=CARTESIAN_POINT('Ctrl Pts',(-23.6508828662191,20.3275266526909,14.8704107892512));
#48488=CARTESIAN_POINT('Ctrl Pts',(-23.5510499836273,20.3259642821496,14.8765817500203));
#48489=CARTESIAN_POINT('Ctrl Pts',(-23.4515086410323,20.3290156253868,14.8827527107893));
#48490=CARTESIAN_POINT('Ctrl Pts',(-23.3755268652506,20.3313447729715,14.8874631210097));
#48491=CARTESIAN_POINT('Ctrl Pts',(-23.2997149478882,20.3363610477618,14.8921735312301));
#48492=CARTESIAN_POINT('Ctrl Pts',(-23.2242751687707,20.3440310294643,14.8968839414505));
#48493=CARTESIAN_POINT('Ctrl Pts',(-23.1254257727498,20.3540810729248,14.9030560327628));
#48494=CARTESIAN_POINT('Ctrl Pts',(-23.0268674893177,20.3687244636739,14.9092281240752));
#48495=CARTESIAN_POINT('Ctrl Pts',(-22.9290612390132,20.3879370919575,14.9154002153875));
#48496=CARTESIAN_POINT('Ctrl Pts',(-22.8313875065087,20.407123689029,14.9215639441263));
#48497=CARTESIAN_POINT('Ctrl Pts',(-22.7344642043974,20.430867135638,14.927727672865));
#48498=CARTESIAN_POINT('Ctrl Pts',(-22.6387476161559,20.4590915278884,14.9338914016038));
#48499=CARTESIAN_POINT('Ctrl Pts',(-22.5431324306561,20.4872860190443,14.9400486004505));
#48500=CARTESIAN_POINT('Ctrl Pts',(-22.4487218318153,20.5199518959084,14.9462057992972));
#48501=CARTESIAN_POINT('Ctrl Pts',(-22.3559614285032,20.556962314669,14.9523629981439));
#48502=CARTESIAN_POINT('Ctrl Pts',(-22.2632688274209,20.5939456810578,14.9585156964516));
#48503=CARTESIAN_POINT('Ctrl Pts',(-22.1722244260074,20.6352671152272,14.9646683947593));
#48504=CARTESIAN_POINT('Ctrl Pts',(-22.0832573081701,20.6807503838195,14.970821093067));
#48505=CARTESIAN_POINT('Ctrl Pts',(-21.9943239267905,20.7262164050916,14.9769714582627));
#48506=CARTESIAN_POINT('Ctrl Pts',(-21.9074666501743,20.7758409274524,14.9831218234585));
#48507=CARTESIAN_POINT('Ctrl Pts',(-21.8230924369732,20.8294005383466,14.9892721886542));
#48508=CARTESIAN_POINT('Ctrl Pts',(-21.7387276460088,20.8829541681323,14.9954218670264));
#48509=CARTESIAN_POINT('Ctrl Pts',(-21.6568457339223,20.9404417799785,15.0015715453986));
#48510=CARTESIAN_POINT('Ctrl Pts',(-21.5778261318149,21.0015956972892,15.0077212237708));
#48511=CARTESIAN_POINT('Ctrl Pts',(-21.4987942140804,21.0627591457646,15.0138718606032));
#48512=CARTESIAN_POINT('Ctrl Pts',(-21.4226258359783,21.1275897687843,15.0200224974357));
#48513=CARTESIAN_POINT('Ctrl Pts',(-21.3496678903753,21.1957791725561,15.0261731342681));
#48514=CARTESIAN_POINT('Ctrl Pts',(-21.2766318950963,21.2640415246657,15.0323303509899));
#48515=CARTESIAN_POINT('Ctrl Pts',(-21.206813508636,21.3356695355718,15.0384875677118));
#48516=CARTESIAN_POINT('Ctrl Pts',(-21.1405231290148,21.4103175400735,15.0446447844336));
#48517=CARTESIAN_POINT('Ctrl Pts',(-21.0741957662625,21.4850071903911,15.0508054362414));
#48518=CARTESIAN_POINT('Ctrl Pts',(-21.011400603143,21.5627198517475,15.0569660880492));
#48519=CARTESIAN_POINT('Ctrl Pts',(-20.9524067303515,21.6430779841118,15.063126739857));
#48520=CARTESIAN_POINT('Ctrl Pts',(-20.8933141398322,21.7235705842074,15.069297700626));
#48521=CARTESIAN_POINT('Ctrl Pts',(-20.8380357860247,21.8067171358415,15.075468661395));
#48522=CARTESIAN_POINT('Ctrl Pts',(-20.7867966167566,21.8921123178713,15.0816396221641));
#48523=CARTESIAN_POINT('Ctrl Pts',(-20.7476847967922,21.9572960636871,15.0863500323845));
#48524=CARTESIAN_POINT('Ctrl Pts',(-20.7109255177076,22.0237894109348,15.0910604426049));
#48525=CARTESIAN_POINT('Ctrl Pts',(-20.6766000032702,22.0914041131179,15.0957708528253));
#48526=CARTESIAN_POINT('Ctrl Pts',(-20.6316229843831,22.1800002430518,15.1019429441377));
#48527=CARTESIAN_POINT('Ctrl Pts',(-20.5906677843335,22.2708343540157,15.10811503545));
#48528=CARTESIAN_POINT('Ctrl Pts',(-20.5539632662718,22.3635056334827,15.1142871267623));
#48529=CARTESIAN_POINT('Ctrl Pts',(-20.5173084792034,22.4560513525276,15.1204508555011));
#48530=CARTESIAN_POINT('Ctrl Pts',(-20.4848930855473,22.5504288922454,15.1266145842399));
#48531=CARTESIAN_POINT('Ctrl Pts',(-20.4568998666447,22.6462133444179,15.1327783129787));
#48532=CARTESIAN_POINT('Ctrl Pts',(-20.4289363039302,22.7418963219531,15.1389355118254));
#48533=CARTESIAN_POINT('Ctrl Pts',(-20.4053857231893,22.8389828340522,15.1450927106721));
#48534=CARTESIAN_POINT('Ctrl Pts',(-20.3863822790797,22.9370294180387,15.1512499095187));
#48535=CARTESIAN_POINT('Ctrl Pts',(-20.3673927253354,23.0350043359179,15.1574026078264));
#48536=CARTESIAN_POINT('Ctrl Pts',(-20.3529437825933,23.133937505301,15.1635553061342));
#48537=CARTESIAN_POINT('Ctrl Pts',(-20.3431191208146,23.2333726690966,15.1697080044419));
#48538=CARTESIAN_POINT('Ctrl Pts',(-20.3332981845617,23.3327701269367,15.1758583696376));
#48539=CARTESIAN_POINT('Ctrl Pts',(-20.3280980876839,23.4326687691357,15.1820087348334));
#48540=CARTESIAN_POINT('Ctrl Pts',(-20.3275508478537,23.5326054505947,15.1881591000291));
#48541=CARTESIAN_POINT('Ctrl Pts',(-20.3270036691347,23.6325309719251,15.1943087784013));
#48542=CARTESIAN_POINT('Ctrl Pts',(-20.331108316819,23.7324940896744,15.2004584567736));
#48543=CARTESIAN_POINT('Ctrl Pts',(-20.3398446886903,23.8320308915428,15.2066081351458));
#48544=CARTESIAN_POINT('Ctrl Pts',(-20.3485824221719,23.9315832067541,15.2127587719783));
#48545=CARTESIAN_POINT('Ctrl Pts',(-20.3619532756917,24.0307086413312,15.2189094088107));
#48546=CARTESIAN_POINT('Ctrl Pts',(-20.3798853026785,24.1289486485667,15.2250600456432));
#48547=CARTESIAN_POINT('Ctrl Pts',(-20.3978365131672,24.2272937519727,15.231217262365));
#48548=CARTESIAN_POINT('Ctrl Pts',(-20.4203585628417,24.3247511083536,15.2373744790869));
#48549=CARTESIAN_POINT('Ctrl Pts',(-20.4473284210579,24.420872727952,15.2435316958087));
#48550=CARTESIAN_POINT('Ctrl Pts',(-20.4743133256475,24.5170479734083,15.2496923476165));
#48551=CARTESIAN_POINT('Ctrl Pts',(-20.5057508437871,24.6118855856704,15.2558529994243));
#48552=CARTESIAN_POINT('Ctrl Pts',(-20.5414687996424,24.7049550978298,15.2620136512321));
#48553=CARTESIAN_POINT('Ctrl Pts',(-20.5772465243392,24.798180348379,15.2681846120012));
#48554=CARTESIAN_POINT('Ctrl Pts',(-20.6173188196338,24.8896311909018,15.2743555727702));
#48555=CARTESIAN_POINT('Ctrl Pts',(-20.6614662758851,24.9788992797562,15.2805265335392));
#48556=CARTESIAN_POINT('Ctrl Pts',(-20.6951648581499,25.0470392880676,15.2852369437596));
#48557=CARTESIAN_POINT('Ctrl Pts',(-20.731236878149,25.113907959357,15.2899473539799));
#48558=CARTESIAN_POINT('Ctrl Pts',(-20.769567865836,25.1793352034948,15.2946577642003));
#48559=CARTESIAN_POINT('Ctrl Pts',(-20.8197891319366,25.2650579890619,15.3008293444124));
#48560=CARTESIAN_POINT('Ctrl Pts',(-20.8740665401047,25.3486072349034,15.3070009246245));
#48561=CARTESIAN_POINT('Ctrl Pts',(-20.9321866452656,25.4295738391929,15.3131725048365));
#48562=CARTESIAN_POINT('Ctrl Pts',(-20.9902317578737,25.5104359720208,15.3193361218395));
#48563=CARTESIAN_POINT('Ctrl Pts',(-21.0521094643142,25.5887217351737,15.3254997388424));
#48564=CARTESIAN_POINT('Ctrl Pts',(-21.1175611014027,25.6640476891033,15.3316633558453));
#48565=CARTESIAN_POINT('Ctrl Pts',(-21.18431301884,25.7408700892947,15.3379494209706));
#48566=CARTESIAN_POINT('Ctrl Pts',(-21.2547821751005,25.8146134150258,15.3442354860958));
#48567=CARTESIAN_POINT('Ctrl Pts',(-21.3286482773805,25.8849028480618,15.3505215512211));
#48568=CARTESIAN_POINT('Ctrl Pts',(-21.4009429475736,25.9536969392964,15.3566738862031));
#48569=CARTESIAN_POINT('Ctrl Pts',(-21.4764911345749,26.0191823187827,15.3628262211852));
#48570=CARTESIAN_POINT('Ctrl Pts',(-21.5549535096008,26.081042798574,15.3689785561672));
#48571=CARTESIAN_POINT('Ctrl Pts',(-21.6359741291018,26.1449202225452,15.3753314863641));
#48572=CARTESIAN_POINT('Ctrl Pts',(-21.7201019028545,26.2049319602866,15.381684416561));
#48573=CARTESIAN_POINT('Ctrl Pts',(-21.8069251862289,26.2607741289247,15.3880373467579));
#48574=CARTESIAN_POINT('Ctrl Pts',(-21.8937484696032,26.3166162975627,15.3943902769548));
#48575=CARTESIAN_POINT('Ctrl Pts',(-21.9832668367093,26.3682886146734,15.4007432071517));
#48576=CARTESIAN_POINT('Ctrl Pts',(-22.0750360153461,26.4155367745563,15.4070961373485));
#48577=CARTESIAN_POINT('Origin',(-23.5502525316942,23.5502525316942,-77.3107734492734));
#48578=CARTESIAN_POINT('',(-22.0738786772418,26.4178312615861,16.9038400528878));
#48579=CARTESIAN_POINT('',(-22.075036069343,26.4155368023571,16.6585071611381));
#48580=CARTESIAN_POINT('',(-22.0750360153461,26.4155367745563,-77.3107734492734));
#48581=CARTESIAN_POINT('',(-26.7773237984114,23.5486249559515,16.0607734492729));
#48582=CARTESIAN_POINT('Ctrl Pts',(-26.7773237984114,23.5486249559515,16.0607734492729));
#48583=CARTESIAN_POINT('Ctrl Pts',(-26.7778921634797,23.4564077062131,16.0664877007678));
#48584=CARTESIAN_POINT('Ctrl Pts',(-26.7324159232951,22.2948726347971,16.1384975893877));
#48585=CARTESIAN_POINT('Ctrl Pts',(-25.3270871613455,20.1778258218927,16.2768031151326));
#48586=CARTESIAN_POINT('Ctrl Pts',(-21.6734278000226,20.2324321416343,16.4756900265074));
#48587=CARTESIAN_POINT('Ctrl Pts',(-19.7444112386102,23.3358340950614,16.6745769378823));
#48588=CARTESIAN_POINT('Ctrl Pts',(-20.8697362492241,25.7041498884009,16.8172936133424));
#48589=CARTESIAN_POINT('Ctrl Pts',(-21.9276889255433,26.3442939038094,16.8937146516776));
#48590=CARTESIAN_POINT('Ctrl Pts',(-22.0738786772418,26.4178312615861,16.9038400528878));
#48591=CARTESIAN_POINT('Ctrl Pts',(-26.7730020461525,23.5484834757995,16.0582900309385));
#48592=CARTESIAN_POINT('Ctrl Pts',(-26.7731762945756,23.8659177764973,16.0398136118881));
#48593=CARTESIAN_POINT('Ctrl Pts',(-26.7264540989983,24.1816697163335,16.0228649312083));
#48594=CARTESIAN_POINT('Ctrl Pts',(-26.6138474838689,24.552984430688,16.0003818521498));
#48595=CARTESIAN_POINT('Ctrl Pts',(-26.5911867086148,24.6197400683399,15.9962420906808));
#48596=CARTESIAN_POINT('Ctrl Pts',(-26.5508597316809,24.7268615417604,15.9894044471309));
#48597=CARTESIAN_POINT('Ctrl Pts',(-26.5345219966239,24.7677038862891,15.9867503428131));
#48598=CARTESIAN_POINT('Ctrl Pts',(-26.514361307108,24.8152566888191,15.9836001378943));
#48599=CARTESIAN_POINT('Ctrl Pts',(-26.5113433459068,24.8223050221252,15.9831316468539));
#48600=CARTESIAN_POINT('Ctrl Pts',(-26.5066857898116,24.8330761750402,15.9824132850001));
#48601=CARTESIAN_POINT('Ctrl Pts',(-26.5050642363678,24.8368068054476,15.982164031655));
#48602=CARTESIAN_POINT('Ctrl Pts',(-26.5020969778309,24.8435982347988,15.9817094610079));
#48603=CARTESIAN_POINT('Ctrl Pts',(-26.5007535624274,24.8466600329974,15.9815042224343));
#48604=CARTESIAN_POINT('Ctrl Pts',(-26.4980453310253,24.8528063892984,15.9810916076277));
#48605=CARTESIAN_POINT('Ctrl Pts',(-26.4966804324778,24.8558909062429,15.9808842287591));
#48606=CARTESIAN_POINT('Ctrl Pts',(-26.4927890198458,24.8646478826211,15.980294592518));
#48607=CARTESIAN_POINT('Ctrl Pts',(-26.4902509600939,24.8703151676267,15.9799119383634));
#48608=CARTESIAN_POINT('Ctrl Pts',(-26.4794584897939,24.8942283748715,15.978292821229));
#48609=CARTESIAN_POINT('Ctrl Pts',(-26.4710506222014,24.9124041742604,15.9770510736214));
#48610=CARTESIAN_POINT('Ctrl Pts',(-26.2965070283962,25.2806784020311,15.9516601379762));
#48611=CARTESIAN_POINT('Ctrl Pts',(-26.0687526282821,25.5979991208634,15.9249424712313));
#48612=CARTESIAN_POINT('Ctrl Pts',(-25.7370288425477,25.9187164459496,15.8942136619572));
#48613=CARTESIAN_POINT('Ctrl Pts',(-25.681972715479,25.9683887249353,15.8893389037841));
#48614=CARTESIAN_POINT('Ctrl Pts',(-25.6062658671256,26.0320950387839,15.882980536931));
#48615=CARTESIAN_POINT('Ctrl Pts',(-25.5870986560268,26.047849580302,15.8813988759047));
#48616=CARTESIAN_POINT('Ctrl Pts',(-25.5604465678583,26.0692454323661,15.8792401930912));
#48617=CARTESIAN_POINT('Ctrl Pts',(-25.553116734926,26.0750773345519,15.878650678345));
#48618=CARTESIAN_POINT('Ctrl Pts',(-25.5405320372317,26.085000922321,15.8776457849238));
#48619=CARTESIAN_POINT('Ctrl Pts',(-25.5352897739234,26.0891083887277,15.8772293234514));
#48620=CARTESIAN_POINT('Ctrl Pts',(-25.5278937547845,26.0948664744263,15.8766448047645));
#48621=CARTESIAN_POINT('Ctrl Pts',(-25.5257506353154,26.0965306326745,15.8764757888738));
#48622=CARTESIAN_POINT('Ctrl Pts',(-25.5222221823097,26.0992633830898,15.8761981115069));
#48623=CARTESIAN_POINT('Ctrl Pts',(-25.5208380812546,26.1003335530305,15.8760893369247));
#48624=CARTESIAN_POINT('Ctrl Pts',(-25.5179457126725,26.1025661358745,15.875862342959));
#48625=CARTESIAN_POINT('Ctrl Pts',(-25.5164372862144,26.1037283392309,15.875744138872));
#48626=CARTESIAN_POINT('Ctrl Pts',(-25.5131160264617,26.1062825955944,15.8754842651549));
#48627=CARTESIAN_POINT('Ctrl Pts',(-25.5113027372233,26.1076740609152,15.8753426376108));
#48628=CARTESIAN_POINT('Ctrl Pts',(-25.5051697836236,26.1123699527427,15.8748644739299));
#48629=CARTESIAN_POINT('Ctrl Pts',(-25.50084320459,26.1156653969009,15.8745285739121));
#48630=CARTESIAN_POINT('Ctrl Pts',(-25.4605395149139,26.1462027767031,15.8714125703997));
#48631=CARTESIAN_POINT('Ctrl Pts',(-25.4240000518611,26.1726988650413,15.8686838841043));
#48632=CARTESIAN_POINT('Ctrl Pts',(-25.3055356294849,26.2548609642573,15.8600978992325));
#48633=CARTESIAN_POINT('Ctrl Pts',(-25.2215918020301,26.3075254403933,15.8544002597142));
#48634=CARTESIAN_POINT('Ctrl Pts',(-25.0799124164264,26.3875597250451,15.8451785731714));
#48635=CARTESIAN_POINT('Ctrl Pts',(-25.0235587237739,26.4172266646204,15.841607374563));
#48636=CARTESIAN_POINT('Ctrl Pts',(-24.8551328753848,26.4996146975565,15.8311182625791));
#48637=CARTESIAN_POINT('Ctrl Pts',(-24.7408615150434,26.5475678767339,15.8242311485049));
#48638=CARTESIAN_POINT('Ctrl Pts',(-24.4600503345786,26.6468095801522,15.8073603647747));
#48639=CARTESIAN_POINT('Ctrl Pts',(-24.2915810314722,26.6914014188752,15.7972691325196));
#48640=CARTESIAN_POINT('Ctrl Pts',(-24.1072813554618,26.7245261174362,15.785893576524));
#48641=CARTESIAN_POINT('Ctrl Pts',(-24.0941970452484,26.7267944038485,15.785084314555));
#48642=CARTESIAN_POINT('Ctrl Pts',(-24.0760826730019,26.7298194979336,15.7839615367968));
#48643=CARTESIAN_POINT('Ctrl Pts',(-24.0710641514428,26.7306453826756,15.7836502202713));
#48644=CARTESIAN_POINT('Ctrl Pts',(-24.062587541198,26.7320197544366,15.7831239485304));
#48645=CARTESIAN_POINT('Ctrl Pts',(-24.0591304638352,26.7325744939895,15.7829091924718));
#48646=CARTESIAN_POINT('Ctrl Pts',(-24.0522868140439,26.7336612226664,15.7824838143815));
#48647=CARTESIAN_POINT('Ctrl Pts',(-24.0489002827755,26.7341934442429,15.7822732000442));
#48648=CARTESIAN_POINT('Ctrl Pts',(-24.0414332847372,26.7353547398381,15.7818085492307));
#48649=CARTESIAN_POINT('Ctrl Pts',(-24.0373524495981,26.7359813773768,15.7815544356708));
#48650=CARTESIAN_POINT('Ctrl Pts',(-24.0230901318942,26.7381433997283,15.780665704856));
#48651=CARTESIAN_POINT('Ctrl Pts',(-24.0129025863662,26.739637818175,15.7800297888816));
#48652=CARTESIAN_POINT('Ctrl Pts',(-23.9082339337787,26.7544796954288,15.7734847074987));
#48653=CARTESIAN_POINT('Ctrl Pts',(-23.813220522853,26.7636723797295,15.7674445014694));
#48654=CARTESIAN_POINT('Ctrl Pts',(-23.552372642849,26.7772638899716,15.750567214016));
#48655=CARTESIAN_POINT('Ctrl Pts',(-23.3863988929209,26.7731001577007,15.7394913032342));
#48656=CARTESIAN_POINT('Ctrl Pts',(-23.0657411463947,26.7402184403829,15.7177103454699));
#48657=CARTESIAN_POINT('Ctrl Pts',(-22.9113481791072,26.7129156773048,15.7070506753344));
#48658=CARTESIAN_POINT('Ctrl Pts',(-22.6961515304407,26.6584522597489,15.6923645106842));
#48659=CARTESIAN_POINT('Ctrl Pts',(-22.6332535893546,26.6404803974442,15.6880953643322));
#48660=CARTESIAN_POINT('Ctrl Pts',(-22.553046589218,26.6148978113509,15.6827180749298));
#48661=CARTESIAN_POINT('Ctrl Pts',(-22.5352010836062,26.6090334944509,15.6815259977277));
#48662=CARTESIAN_POINT('Ctrl Pts',(-22.5101782080147,26.6005674674096,15.6798615836035));
#48663=CARTESIAN_POINT('Ctrl Pts',(-22.5029576494625,26.598095906646,15.6793821402659));
#48664=CARTESIAN_POINT('Ctrl Pts',(-22.4920292778801,26.5943117585682,15.6786578424772));
#48665=CARTESIAN_POINT('Ctrl Pts',(-22.48831503777,26.593018015759,15.678411910174));
#48666=CARTESIAN_POINT('Ctrl Pts',(-22.4814818345048,26.5906238409219,15.6779599073608));
#48667=CARTESIAN_POINT('Ctrl Pts',(-22.4783621854736,26.5895254031322,15.6777537203965));
#48668=CARTESIAN_POINT('Ctrl Pts',(-22.4733254344228,26.5877432283603,15.6774211102004));
#48669=CARTESIAN_POINT('Ctrl Pts',(-22.4714072898055,26.5870624778844,15.6772945089123));
#48670=CARTESIAN_POINT('Ctrl Pts',(-22.4677197504036,26.5857498336116,15.6770512539575));
#48671=CARTESIAN_POINT('Ctrl Pts',(-22.4659502762978,26.5851182143027,15.6769345853124));
#48672=CARTESIAN_POINT('Ctrl Pts',(-22.4619228705945,26.5836766473545,15.6766691721931));
#48673=CARTESIAN_POINT('Ctrl Pts',(-22.459665293269,26.5828657269719,15.6765204869486));
#48674=CARTESIAN_POINT('Ctrl Pts',(-22.4526549359712,26.5803387703929,15.6760590641566));
#48675=CARTESIAN_POINT('Ctrl Pts',(-22.4479052555735,26.5786140655506,15.6757468439657));
#48676=CARTESIAN_POINT('Ctrl Pts',(-22.4118273264727,26.5654173162887,15.6733781982146));
#48677=CARTESIAN_POINT('Ctrl Pts',(-22.3806733919683,26.5534700521566,15.6713496813345));
#48678=CARTESIAN_POINT('Ctrl Pts',(-22.2561677256447,26.5034917679209,15.663289442689));
#48679=CARTESIAN_POINT('Ctrl Pts',(-22.1645124296855,26.4616044966735,15.6574615682194));
#48680=CARTESIAN_POINT('Ctrl Pts',(-22.0750357147148,26.4155366197736,15.6517373095584));
#48681=CARTESIAN_POINT('',(-26.7730019920283,23.5483874803723,15.8142265507266));
#48682=CARTESIAN_POINT('Ctrl Pts',(-22.0750360153461,26.4155367745563,15.4070961373485));
#48683=CARTESIAN_POINT('Ctrl Pts',(-22.163885353475,26.4612816291552,15.4132469349427));
#48684=CARTESIAN_POINT('Ctrl Pts',(-22.2548440136306,26.5028794401595,15.4193977325368));
#48685=CARTESIAN_POINT('Ctrl Pts',(-22.3474855442512,26.5401470342507,15.4255485301309));
#48686=CARTESIAN_POINT('Ctrl Pts',(-22.4402273622975,26.5774549717067,15.4317059861605));
#48687=CARTESIAN_POINT('Ctrl Pts',(-22.5346552845119,26.6104231702702,15.4378634421901));
#48688=CARTESIAN_POINT('Ctrl Pts',(-22.6303246422378,26.6389173307134,15.4440208982197));
#48689=CARTESIAN_POINT('Ctrl Pts',(-22.726049365229,26.6674279811466,15.4501819176597));
#48690=CARTESIAN_POINT('Ctrl Pts',(-22.8230165328247,26.6914593331419,15.4563429370998));
#48691=CARTESIAN_POINT('Ctrl Pts',(-22.9207701789003,26.7109280180453,15.4625039565398));
#48692=CARTESIAN_POINT('Ctrl Pts',(-23.0186848355554,26.7304287699291,15.4686751238296));
#48693=CARTESIAN_POINT('Ctrl Pts',(-23.1173881283593,26.7453517808918,15.4748462911193));
#48694=CARTESIAN_POINT('Ctrl Pts',(-23.2164177695234,26.7556654402079,15.4810174584091));
#48695=CARTESIAN_POINT('Ctrl Pts',(-23.2834264764393,26.7626442090515,15.4851931974644));
#48696=CARTESIAN_POINT('Ctrl Pts',(-23.3505845259072,26.7675136305882,15.4893689365198));
#48697=CARTESIAN_POINT('Ctrl Pts',(-23.4177491731461,26.7702774419198,15.4935446755752));
#48698=CARTESIAN_POINT('Ctrl Pts',(-23.5170241350681,26.7743625860541,15.4997167668875));
#48699=CARTESIAN_POINT('Ctrl Pts',(-23.6166630386624,26.7738595788928,15.5058888581998));
#48700=CARTESIAN_POINT('Ctrl Pts',(-23.7162062091023,26.7687268502891,15.5120609495121));
#48701=CARTESIAN_POINT('Ctrl Pts',(-23.8156145083873,26.7636010760252,15.5182246782509));
#48702=CARTESIAN_POINT('Ctrl Pts',(-23.9149269023268,26.7538580703781,15.5243884069897));
#48703=CARTESIAN_POINT('Ctrl Pts',(-24.0136809531081,26.7395081910489,15.5305521357285));
#48704=CARTESIAN_POINT('Ctrl Pts',(-24.112330383241,26.72517351407,15.5367093345751));
#48705=CARTESIAN_POINT('Ctrl Pts',(-24.2104222186818,26.7062417285075,15.5428665334218));
#48706=CARTESIAN_POINT('Ctrl Pts',(-24.3074973562965,26.6827751314711,15.5490237322685));
#48707=CARTESIAN_POINT('Ctrl Pts',(-24.4045015378728,26.659325687094,15.5551764305762));
#48708=CARTESIAN_POINT('Ctrl Pts',(-24.5004900781541,26.6313481231318,15.5613291288839));
#48709=CARTESIAN_POINT('Ctrl Pts',(-24.5950132198864,26.598955971996,15.5674818271916));
#48710=CARTESIAN_POINT('Ctrl Pts',(-24.6895005183089,26.5665761040101,15.5736321923874));
#48711=CARTESIAN_POINT('Ctrl Pts',(-24.7825231118306,26.5297851157756,15.5797825575831));
#48712=CARTESIAN_POINT('Ctrl Pts',(-24.8736464464446,26.4887463821049,15.5859329227789));
#48713=CARTESIAN_POINT('Ctrl Pts',(-24.9647596051343,26.4477122313114,15.5920826011511));
#48714=CARTESIAN_POINT('Ctrl Pts',(-25.0539735305013,26.4024314565456,15.5982322795233));
#48715=CARTESIAN_POINT('Ctrl Pts',(-25.1408746332202,26.3531151563401,15.6043819578956));
#48716=CARTESIAN_POINT('Ctrl Pts',(-25.2277892799402,26.3037911699258,15.610532594728));
#48717=CARTESIAN_POINT('Ctrl Pts',(-25.3123900101946,26.250430623224,15.6166832315605));
#48718=CARTESIAN_POINT('Ctrl Pts',(-25.3942896628079,26.1932895389217,15.6228338683929));
#48719=CARTESIAN_POINT('Ctrl Pts',(-25.476276930845,26.1360873256626,15.6289910851147));
#48720=CARTESIAN_POINT('Ctrl Pts',(-25.5555569940663,26.0750967476206,15.6351483018365));
#48721=CARTESIAN_POINT('Ctrl Pts',(-25.6317735251724,26.0106159024607,15.6413055185584));
#48722=CARTESIAN_POINT('Ctrl Pts',(-25.7080325771692,25.9460990837013,15.6474661703662));
#48723=CARTESIAN_POINT('Ctrl Pts',(-25.7812243751031,25.8780884157034,15.653626822174));
#48724=CARTESIAN_POINT('Ctrl Pts',(-25.8510289554246,25.806919412407,15.6597874739818));
#48725=CARTESIAN_POINT('Ctrl Pts',(-25.9209503436319,25.7356313180602,15.6659584347508));
#48726=CARTESIAN_POINT('Ctrl Pts',(-25.9874729029315,25.6611746558161,15.6721293955199));
#48727=CARTESIAN_POINT('Ctrl Pts',(-26.05031642152,25.5839187061902,15.6783003562889));
#48728=CARTESIAN_POINT('Ctrl Pts',(-26.0982860592022,25.5249477892907,15.6830107665093));
#48729=CARTESIAN_POINT('Ctrl Pts',(-26.1441129048545,25.4643465513133,15.6877211767296));
#48730=CARTESIAN_POINT('Ctrl Pts',(-26.1876898325281,25.4022898009386,15.69243158695));
#48731=CARTESIAN_POINT('Ctrl Pts',(-26.2454387822507,25.3200510487213,15.6986739096081));
#48732=CARTESIAN_POINT('Ctrl Pts',(-26.2994360637396,25.2349687783033,15.7049162322662));
#48733=CARTESIAN_POINT('Ctrl Pts',(-26.3493933091914,25.1474151628162,15.7111585549243));
#48734=CARTESIAN_POINT('Ctrl Pts',(-26.399279228004,25.0599865523226,15.7173919650835));
#48735=CARTESIAN_POINT('Ctrl Pts',(-26.4451363713419,24.9700939741101,15.7236253752428));
#48736=CARTESIAN_POINT('Ctrl Pts',(-26.4867185018539,24.8781400151031,15.729858785402));
#48737=CARTESIAN_POINT('Ctrl Pts',(-26.5282515144078,24.7862946746457,15.7360848324854));
#48738=CARTESIAN_POINT('Ctrl Pts',(-26.5655193832855,24.6923931770856,15.7423108795688));
#48739=CARTESIAN_POINT('Ctrl Pts',(-26.5983212629338,24.596863525397,15.7485369266522));
#48740=CARTESIAN_POINT('Ctrl Pts',(-26.631088380122,24.5014351132025,15.7547563755553));
#48741=CARTESIAN_POINT('Ctrl Pts',(-26.6593987923052,24.4043823783789,15.7609758244585));
#48742=CARTESIAN_POINT('Ctrl Pts',(-26.6830997521404,24.3061532234802,15.7671952733617));
#48743=CARTESIAN_POINT('Ctrl Pts',(-26.7067859713451,24.207985161452,15.7734108541262));
#48744=CARTESIAN_POINT('Ctrl Pts',(-26.7258683414404,24.1086425433305,15.7796264348908));
#48745=CARTESIAN_POINT('Ctrl Pts',(-26.7402441209884,24.0085878049735,15.7858420156554));
#48746=CARTESIAN_POINT('Ctrl Pts',(-26.7546153903739,23.9085644571325,15.7920556463845));
#48747=CARTESIAN_POINT('Ctrl Pts',(-26.7642829443631,23.8078298499944,15.7982692771136));
#48748=CARTESIAN_POINT('Ctrl Pts',(-26.7691953950023,23.7068552304513,15.8044829078427));
#48749=CARTESIAN_POINT('Ctrl Pts',(-26.7717631457426,23.6540755338959,15.807730788804));
#48750=CARTESIAN_POINT('Ctrl Pts',(-26.77303257297,23.6012303765799,15.8109786697653));
#48751=CARTESIAN_POINT('Ctrl Pts',(-26.7730019920283,23.5483874803723,15.8142265507266));
#48752=CARTESIAN_POINT('Ctrl Pts',(-26.7730018961391,23.5482285578474,15.8117750777804));
#48753=CARTESIAN_POINT('Ctrl Pts',(-26.7728046263283,23.2341181960848,15.8321379522218));
#48754=CARTESIAN_POINT('Ctrl Pts',(-26.7266920806876,22.921780688606,15.8538922170526));
#48755=CARTESIAN_POINT('Ctrl Pts',(-26.6171748740879,22.558066115835,15.8790274192304));
#48756=CARTESIAN_POINT('Ctrl Pts',(-26.5962785012017,22.4956561139789,15.8833234263691));
#48757=CARTESIAN_POINT('Ctrl Pts',(-26.5636287593405,22.4072342349994,15.8893442082632));
#48758=CARTESIAN_POINT('Ctrl Pts',(-26.5534195926227,22.3806736086413,15.8911440443552));
#48759=CARTESIAN_POINT('Ctrl Pts',(-26.5412092483208,22.3501211816968,15.8932013752921));
#48760=CARTESIAN_POINT('Ctrl Pts',(-26.5395503688379,22.3459951757296,15.8934789349227));
#48761=CARTESIAN_POINT('Ctrl Pts',(-26.5370198851222,22.3397387411227,15.8938993759731));
#48762=CARTESIAN_POINT('Ctrl Pts',(-26.5361545385679,22.3376058122847,15.8940426350278));
#48763=CARTESIAN_POINT('Ctrl Pts',(-26.5345837512811,22.33374597021,15.8943017415655));
#48764=CARTESIAN_POINT('Ctrl Pts',(-26.5338790984175,22.33201874759,15.8944176364623));
#48765=CARTESIAN_POINT('Ctrl Pts',(-26.5324602414214,22.3285495059147,15.8946503154213));
#48766=CARTESIAN_POINT('Ctrl Pts',(-26.5317460133275,22.3268075079281,15.8947670973482));
#48767=CARTESIAN_POINT('Ctrl Pts',(-26.5297062122066,22.3218448395999,15.8950996435703));
#48768=CARTESIAN_POINT('Ctrl Pts',(-26.5283769391468,22.3186256781698,15.8953151822458));
#48769=CARTESIAN_POINT('Ctrl Pts',(-26.5226881611175,22.3049119630758,15.8962326583744));
#48770=CARTESIAN_POINT('Ctrl Pts',(-26.5182783134091,22.2944381859082,15.8969315653357));
#48771=CARTESIAN_POINT('Ctrl Pts',(-26.4365297888622,22.1031142941592,15.9096691081607));
#48772=CARTESIAN_POINT('Ctrl Pts',(-26.3428363640157,21.9296642434892,15.9207480771629));
#48773=CARTESIAN_POINT('Ctrl Pts',(-26.1429810057039,21.6290979916271,15.9409467374906));
#48774=CARTESIAN_POINT('Ctrl Pts',(-26.0417556556983,21.4995245614739,15.9500594765916));
#48775=CARTESIAN_POINT('Ctrl Pts',(-25.8889610684588,21.3320393289377,15.9630482950718));
#48776=CARTESIAN_POINT('Ctrl Pts',(-25.8454851776859,21.2870835365266,15.9666685772429));
#48777=CARTESIAN_POINT('Ctrl Pts',(-25.7620089369155,21.2056464709397,15.9735154644692));
#48778=CARTESIAN_POINT('Ctrl Pts',(-25.7223438230463,21.1688531752513,15.9767281623027));
#48779=CARTESIAN_POINT('Ctrl Pts',(-25.6670583362606,21.1201011685873,15.981163379127));
#48780=CARTESIAN_POINT('Ctrl Pts',(-25.6522255844581,21.1072601614108,15.9823492686703));
#48781=CARTESIAN_POINT('Ctrl Pts',(-25.626890928256,21.0857289860596,15.9843685178538));
#48782=CARTESIAN_POINT('Ctrl Pts',(-25.6164493334037,21.0769684589018,15.985198970323));
#48783=CARTESIAN_POINT('Ctrl Pts',(-25.6020002200609,21.0650009703118,15.9863458515667));
#48784=CARTESIAN_POINT('Ctrl Pts',(-25.5980400401563,21.0617368657247,15.9866599502281));
#48785=CARTESIAN_POINT('Ctrl Pts',(-25.591650143486,21.0564956940417,15.9871663881908));
#48786=CARTESIAN_POINT('Ctrl Pts',(-25.5892253001927,21.0545126766654,15.9873584858278));
#48787=CARTESIAN_POINT('Ctrl Pts',(-25.5841679473789,21.0503891041346,15.9877589559783));
#48788=CARTESIAN_POINT('Ctrl Pts',(-25.5815349420605,21.048249165628,15.9879673530847));
#48789=CARTESIAN_POINT('Ctrl Pts',(-25.5754577119258,21.0433258973237,15.9884481278494));
#48790=CARTESIAN_POINT('Ctrl Pts',(-25.572011125737,21.0405455051164,15.9887206234925));
#48791=CARTESIAN_POINT('Ctrl Pts',(-25.5612736199777,21.031919934766,15.9895690478977));
#48792=CARTESIAN_POINT('Ctrl Pts',(-25.5539630491226,21.0260993973405,15.9901459649327));
#48793=CARTESIAN_POINT('Ctrl Pts',(-25.4919343253948,20.9771525862421,15.9950350486004));
#48794=CARTESIAN_POINT('Ctrl Pts',(-25.4358599983036,20.9357822649959,15.9994165019083));
#48795=CARTESIAN_POINT('Ctrl Pts',(-25.3726372178957,20.8922303022475,16.0043210452401));
#48796=CARTESIAN_POINT('Ctrl Pts',(-25.3667685945868,20.8882161854501,16.0047759728684));
#48797=CARTESIAN_POINT('Ctrl Pts',(-25.2447915163293,20.8053754849056,16.0142245766527));
#48798=CARTESIAN_POINT('Ctrl Pts',(-25.1236837315748,20.7342059427412,16.0234868806989));
#48799=CARTESIAN_POINT('Ctrl Pts',(-24.9114186690282,20.6274439134964,16.0394321673669));
#48800=CARTESIAN_POINT('Ctrl Pts',(-24.8225673036688,20.5876864548579,16.0460247431171));
#48801=CARTESIAN_POINT('Ctrl Pts',(-24.552109253191,20.4810812344191,16.065696558887));
#48802=CARTESIAN_POINT('Ctrl Pts',(-24.3661168695984,20.4264864061892,16.0787277483863));
#48803=CARTESIAN_POINT('Ctrl Pts',(-24.168604770611,20.3873709206322,16.0913685036925));
#48804=CARTESIAN_POINT('Ctrl Pts',(-24.160874195007,20.3858693746855,16.0918613554545));
#48805=CARTESIAN_POINT('Ctrl Pts',(-24.1502857383422,20.3838529762968,16.0925337296076));
#48806=CARTESIAN_POINT('Ctrl Pts',(-24.1474326332544,20.383313643752,16.0927146379334));
#48807=CARTESIAN_POINT('Ctrl Pts',(-24.1426489033622,20.3824160528144,16.0930175124967));
#48808=CARTESIAN_POINT('Ctrl Pts',(-24.1407186802346,20.3820557029658,16.0931395989234));
#48809=CARTESIAN_POINT('Ctrl Pts',(-24.1369094771843,20.3813481718437,16.093380286931));
#48810=CARTESIAN_POINT('Ctrl Pts',(-24.1350305174239,20.3810008974731,16.0934988937221));
#48811=CARTESIAN_POINT('Ctrl Pts',(-24.1308788305256,20.3802373894404,16.0937607070686));
#48812=CARTESIAN_POINT('Ctrl Pts',(-24.1286059585695,20.3798219277047,16.0939038691588));
#48813=CARTESIAN_POINT('Ctrl Pts',(-24.1208446038823,20.3784118417686,16.0943921632216));
#48814=CARTESIAN_POINT('Ctrl Pts',(-24.1153539463309,20.3774290151097,16.0947366222004));
#48815=CARTESIAN_POINT('Ctrl Pts',(-24.0610541735627,20.3678547908458,16.0981337322372));
#48816=CARTESIAN_POINT('Ctrl Pts',(-24.0120522970798,20.3603755218276,16.1011242782874));
#48817=CARTESIAN_POINT('Ctrl Pts',(-23.9573550715616,20.3533139527502,16.1043985952163));
#48818=CARTESIAN_POINT('Ctrl Pts',(-23.9518140873578,20.3526132347569,16.1047295667845));
#48819=CARTESIAN_POINT('Ctrl Pts',(-23.9424677781203,20.3514559687116,16.1052866543154));
#48820=CARTESIAN_POINT('Ctrl Pts',(-23.9386634286815,20.3509918004893,16.1055130829104));
#48821=CARTESIAN_POINT('Ctrl Pts',(-23.6839352924637,20.3203735107428,16.1206525324504));
#48822=CARTESIAN_POINT('Ctrl Pts',(-23.4303091735725,20.3198295495388,16.1343854323784));
#48823=CARTESIAN_POINT('Ctrl Pts',(-23.0677411940706,20.3618530963051,16.154960166579));
#48824=CARTESIAN_POINT('Ctrl Pts',(-22.9570375205518,20.3805835952993,16.1613625019256));
#48825=CARTESIAN_POINT('Ctrl Pts',(-22.7898196956833,20.4179438469617,16.1713903776175));
#48826=CARTESIAN_POINT('Ctrl Pts',(-22.7324658839398,20.4324263426966,16.1748947941917));
#48827=CARTESIAN_POINT('Ctrl Pts',(-22.655366143927,20.4541686332814,16.1797096000117));
#48828=CARTESIAN_POINT('Ctrl Pts',(-22.6352431548661,20.4600559422142,16.1809759395686));
#48829=CARTESIAN_POINT('Ctrl Pts',(-22.6059026853705,20.4689516865248,16.1828370969296));
#48830=CARTESIAN_POINT('Ctrl Pts',(-22.5966387889225,20.4718061122993,16.183426898248));
#48831=CARTESIAN_POINT('Ctrl Pts',(-22.5800311541497,20.4770054754259,16.1844882015277));
#48832=CARTESIAN_POINT('Ctrl Pts',(-22.5726826570633,20.4793350582195,16.1849591975514));
#48833=CARTESIAN_POINT('Ctrl Pts',(-22.5614771997892,20.4829316507903,16.1856795566684));
#48834=CARTESIAN_POINT('Ctrl Pts',(-22.5576141223763,20.4841796311387,16.1859282920167));
#48835=CARTESIAN_POINT('Ctrl Pts',(-22.5506047118037,20.486458680728,16.1863803288407));
#48836=CARTESIAN_POINT('Ctrl Pts',(-22.5474575852717,20.487487307207,16.186583549398));
#48837=CARTESIAN_POINT('Ctrl Pts',(-22.5411568109731,20.489557444106,16.1869909397812));
#48838=CARTESIAN_POINT('Ctrl Pts',(-22.5380031768769,20.4905989832829,16.1871951103564));
#48839=CARTESIAN_POINT('Ctrl Pts',(-22.5292024394174,20.4935206663934,16.1877656267725));
#48840=CARTESIAN_POINT('Ctrl Pts',(-22.5235589475374,20.4954115749872,16.1881323286722));
#48841=CARTESIAN_POINT('Ctrl Pts',(-22.5008637480211,20.5030858228637,16.1896104913225));
#48842=CARTESIAN_POINT('Ctrl Pts',(-22.4838556624521,20.5089963000042,16.1907261631966));
#48843=CARTESIAN_POINT('Ctrl Pts',(-22.238943061262,20.5964128761868,16.2069083962712));
#48844=CARTESIAN_POINT('Ctrl Pts',(-22.0209283932317,20.7031798509227,16.2228694379229));
#48845=CARTESIAN_POINT('Ctrl Pts',(-21.6897723810268,20.9144433432028,16.2493873880407));
#48846=CARTESIAN_POINT('Ctrl Pts',(-21.5684413600974,21.004412244643,16.259661852537));
#48847=CARTESIAN_POINT('Ctrl Pts',(-21.3807788396897,21.1651405073939,16.2760967010109));
#48848=CARTESIAN_POINT('Ctrl Pts',(-21.3105320186083,21.230978623866,16.2823883777088));
#48849=CARTESIAN_POINT('Ctrl Pts',(-21.2371432988625,21.3062111442115,16.2890219083685));
#48850=CARTESIAN_POINT('Ctrl Pts',(-21.2309822508871,21.3125793114501,16.2895792801893));
#48851=CARTESIAN_POINT('Ctrl Pts',(-21.2204005971008,21.3236073470871,16.2905372742825));
#48852=CARTESIAN_POINT('Ctrl Pts',(-21.2159675512014,21.3282551314257,16.2909388285018));
#48853=CARTESIAN_POINT('Ctrl Pts',(-21.2097078788499,21.3348574322945,16.291506106839));
#48854=CARTESIAN_POINT('Ctrl Pts',(-21.2078697828678,21.3368009789089,16.2916727154789));
#48855=CARTESIAN_POINT('Ctrl Pts',(-21.2047183466866,21.3401415331483,16.2919584201328));
#48856=CARTESIAN_POINT('Ctrl Pts',(-21.2034038315663,21.3415374260929,16.2920776078245));
#48857=CARTESIAN_POINT('Ctrl Pts',(-21.200891551821,21.3442100086932,16.2923054259543));
#48858=CARTESIAN_POINT('Ctrl Pts',(-21.1996935832901,21.3454864994013,16.292414072509));
#48859=CARTESIAN_POINT('Ctrl Pts',(-21.1968799906056,21.3484894118067,16.2926692751785));
#48860=CARTESIAN_POINT('Ctrl Pts',(-21.1952652224529,21.3502166395682,16.2928157646713));
#48861=CARTESIAN_POINT('Ctrl Pts',(-21.190519176012,21.3553044341759,16.2932463967786));
#48862=CARTESIAN_POINT('Ctrl Pts',(-21.1873931628272,21.3586699381573,16.2935301347626));
#48863=CARTESIAN_POINT('Ctrl Pts',(-21.1608849768732,21.3873316199847,16.295937161982));
#48864=CARTESIAN_POINT('Ctrl Pts',(-21.1379014396724,21.4129957326738,16.2980305477768));
#48865=CARTESIAN_POINT('Ctrl Pts',(-21.1115917740185,21.4433391777641,16.3004413494327));
#48866=CARTESIAN_POINT('Ctrl Pts',(-21.1078622827492,21.4476636406365,16.300783436523));
#48867=CARTESIAN_POINT('Ctrl Pts',(-20.9034181048028,21.6860010726898,16.3195566678349));
#48868=CARTESIAN_POINT('Ctrl Pts',(-20.7372799891048,21.9476264136509,16.3360382288832));
#48869=CARTESIAN_POINT('Ctrl Pts',(-20.5695687409252,22.3207109646318,16.359312903484));
#48870=CARTESIAN_POINT('Ctrl Pts',(-20.5326273929913,22.4143897292331,16.3651257639763));
#48871=CARTESIAN_POINT('Ctrl Pts',(-20.4862942302259,22.5501957876227,16.3736127145109));
#48872=CARTESIAN_POINT('Ctrl Pts',(-20.4732679082469,22.5910240219667,16.3761713397166));
#48873=CARTESIAN_POINT('Ctrl Pts',(-20.4563592655472,22.6479143148062,16.379751794366));
#48874=CARTESIAN_POINT('Ctrl Pts',(-20.4517801593,22.6637657907418,16.3807510367652));
#48875=CARTESIAN_POINT('Ctrl Pts',(-20.4451299067435,22.6874681115356,16.3822478508855));
#48876=CARTESIAN_POINT('Ctrl Pts',(-20.4429663315177,22.6952929186405,16.3827424238359));
#48877=CARTESIAN_POINT('Ctrl Pts',(-20.4390779389906,22.7095654532638,16.3836453529233));
#48878=CARTESIAN_POINT('Ctrl Pts',(-20.4373435369129,22.7160105408574,16.3840533958741));
#48879=CARTESIAN_POINT('Ctrl Pts',(-20.43464622549,22.7261593623094,16.3846964199982));
#48880=CARTESIAN_POINT('Ctrl Pts',(-20.4336698637091,22.7298595280059,16.3849309639778));
#48881=CARTESIAN_POINT('Ctrl Pts',(-20.4319323877105,22.7364919896466,16.3853515670648));
#48882=CARTESIAN_POINT('Ctrl Pts',(-20.4311688120609,22.739423640998,16.3855375460546));
#48883=CARTESIAN_POINT('Ctrl Pts',(-20.4295583925683,22.7456425790151,16.3859322064378));
#48884=CARTESIAN_POINT('Ctrl Pts',(-20.4287126071909,22.7489301337069,16.3861409218915));
#48885=CARTESIAN_POINT('Ctrl Pts',(-20.4263079516749,22.7583385724532,16.3867384739902));
#48886=CARTESIAN_POINT('Ctrl Pts',(-20.4247618861351,22.76446268607,16.3871277247842));
#48887=CARTESIAN_POINT('Ctrl Pts',(-20.4181745419809,22.7908828114572,16.3888082948649));
#48888=CARTESIAN_POINT('Ctrl Pts',(-20.4133129706029,22.8112227200402,16.3901054078012));
#48889=CARTESIAN_POINT('Ctrl Pts',(-20.3236170564444,23.2033344889079,16.4151788063718));
#48890=CARTESIAN_POINT('Ctrl Pts',(-20.3052567811658,23.5871522308096,16.4414266759297));
#48891=CARTESIAN_POINT('Ctrl Pts',(-20.3614447576155,24.020031485543,16.4705448497468));
#48892=CARTESIAN_POINT('Ctrl Pts',(-20.3699926179472,24.0747854490492,16.474208191151));
#48893=CARTESIAN_POINT('Ctrl Pts',(-20.3862101741792,24.1635779747463,16.4800899704882));
#48894=CARTESIAN_POINT('Ctrl Pts',(-20.3930279092952,24.1977593167627,16.4823397899832));
#48895=CARTESIAN_POINT('Ctrl Pts',(-20.4060283107048,24.2578400475598,16.4862610472686));
#48896=CARTESIAN_POINT('Ctrl Pts',(-20.4119798587934,24.2837856174466,16.4879433807958));
#48897=CARTESIAN_POINT('Ctrl Pts',(-20.4192823851471,24.3139033742627,16.4898809808332));
#48898=CARTESIAN_POINT('Ctrl Pts',(-20.4203210020499,24.3181491967485,16.4901537775683));
#48899=CARTESIAN_POINT('Ctrl Pts',(-20.4219159178755,24.3246121497252,16.4905684720561));
#48900=CARTESIAN_POINT('Ctrl Pts',(-20.4224659376056,24.3268308016153,16.4907107319728));
#48901=CARTESIAN_POINT('Ctrl Pts',(-20.4234689031042,24.3308581805945,16.4909687842031));
#48902=CARTESIAN_POINT('Ctrl Pts',(-20.4239210565671,24.3326670936724,16.4910846220363));
#48903=CARTESIAN_POINT('Ctrl Pts',(-20.4249047552221,24.3365880719622,16.4913355645832));
#48904=CARTESIAN_POINT('Ctrl Pts',(-20.4254368701059,24.3386999852049,16.4914706353187));
#48905=CARTESIAN_POINT('Ctrl Pts',(-20.42689564839,24.3444650638738,16.4918391036701));
#48906=CARTESIAN_POINT('Ctrl Pts',(-20.4278265835876,24.348117160369,16.4920722529825));
#48907=CARTESIAN_POINT('Ctrl Pts',(-20.4323457858973,24.3657171262349,16.4931945660176));
#48908=CARTESIAN_POINT('Ctrl Pts',(-20.4360211891225,24.3796427556997,16.4940787375349));
#48909=CARTESIAN_POINT('Ctrl Pts',(-20.5044369579604,24.6319929870953,16.5100390938856));
#48910=CARTESIAN_POINT('Ctrl Pts',(-20.596300950982,24.8622617147293,16.5236358568257));
#48911=CARTESIAN_POINT('Ctrl Pts',(-20.7825040977251,25.2075892230795,16.5455764208667));
#48912=CARTESIAN_POINT('Ctrl Pts',(-20.8599632540827,25.3305714729923,16.5537392769632));
#48913=CARTESIAN_POINT('Ctrl Pts',(-20.9980124017785,25.5200642275414,16.5673467523794));
#48914=CARTESIAN_POINT('Ctrl Pts',(-21.0535524555293,25.5900011333779,16.5726195010925));
#48915=CARTESIAN_POINT('Ctrl Pts',(-21.1219830814292,25.6691819488672,16.5789390759949));
#48916=CARTESIAN_POINT('Ctrl Pts',(-21.132129049664,25.6807532266075,16.5798717415497));
#48917=CARTESIAN_POINT('Ctrl Pts',(-21.1474834237992,25.6980136119804,16.5812769833772));
#48918=CARTESIAN_POINT('Ctrl Pts',(-21.1526301087282,25.7037575256785,16.5817469810553));
#48919=CARTESIAN_POINT('Ctrl Pts',(-21.1609474455475,25.712973242686,16.5825048997269));
#48920=CARTESIAN_POINT('Ctrl Pts',(-21.1641051849347,25.7164567020401,16.5827922756422));
#48921=CARTESIAN_POINT('Ctrl Pts',(-21.1701573225114,25.7231038252824,16.5833423559056));
#48922=CARTESIAN_POINT('Ctrl Pts',(-21.1730504359872,25.7262686494441,16.5836050054352));
#48923=CARTESIAN_POINT('Ctrl Pts',(-21.1781890537828,25.7318673889729,16.5840709747375));
#48924=CARTESIAN_POINT('Ctrl Pts',(-21.1804320139563,25.734303639685,16.5842741858061));
#48925=CARTESIAN_POINT('Ctrl Pts',(-21.1848613711635,25.7390998470488,16.5846751307482));
#48926=CARTESIAN_POINT('Ctrl Pts',(-21.1870475553137,25.7414599960242,16.5848728553873));
#48927=CARTESIAN_POINT('Ctrl Pts',(-21.1923137503684,25.7471281985788,16.5853487427258));
#48928=CARTESIAN_POINT('Ctrl Pts',(-21.1953971878599,25.7504330473613,16.5856270524828));
#48929=CARTESIAN_POINT('Ctrl Pts',(-21.2048640331644,25.7605369769652,16.5864805271361));
#48930=CARTESIAN_POINT('Ctrl Pts',(-21.2112699675271,25.767314799568,16.5870566633853));
#48931=CARTESIAN_POINT('Ctrl Pts',(-21.2852088855516,25.8448690250561,16.5936909928919));
#48932=CARTESIAN_POINT('Ctrl Pts',(-21.3558947246034,25.9125560747297,16.5998873210614));
#48933=CARTESIAN_POINT('Ctrl Pts',(-21.6041877538224,26.1295440309248,16.6212151733245));
#48934=CARTESIAN_POINT('Ctrl Pts',(-21.7947785989043,26.2628519286952,16.6369461197535));
#48935=CARTESIAN_POINT('Ctrl Pts',(-22.023487943234,26.3885538358758,16.6545854676908));
#48936=CARTESIAN_POINT('Ctrl Pts',(-22.0491739137977,26.4022214472271,16.6565491544851));
#48937=CARTESIAN_POINT('Ctrl Pts',(-22.075036069343,26.4155368023571,16.6585071611381));
#48938=CARTESIAN_POINT('Origin',(-23.5502525316942,23.5502525316942,-77.3107734492734));
#48939=CARTESIAN_POINT('',(-22.0750359582753,26.4155367451729,18.1566419298442));
#48940=CARTESIAN_POINT('',(-22.075036043603,26.4155367891046,17.9090429972639));
#48941=CARTESIAN_POINT('',(-22.0750360153461,26.4155367745563,-77.3107734492734));
#48942=CARTESIAN_POINT('',(-26.7741131953272,23.5531281751,17.3107734492729));
#48943=CARTESIAN_POINT('Ctrl Pts',(-22.0750359582753,26.4155367451729,18.1566419298442));
#48944=CARTESIAN_POINT('Ctrl Pts',(-21.9853865332552,26.3693799566194,18.1502524745867));
#48945=CARTESIAN_POINT('Ctrl Pts',(-21.8979439411704,26.3190367025206,18.1437182804855));
#48946=CARTESIAN_POINT('Ctrl Pts',(-21.5963525737374,26.1260149599978,18.1201039190352));
#48947=CARTESIAN_POINT('Ctrl Pts',(-21.3971129691064,25.961942231366,18.1023842227795));
#48948=CARTESIAN_POINT('Ctrl Pts',(-21.1502391614448,25.7034156973081,18.0786444313708));
#48949=CARTESIAN_POINT('Ctrl Pts',(-21.0843914208312,25.6276811021549,18.0721070584265));
#48950=CARTESIAN_POINT('Ctrl Pts',(-21.0181042130766,25.5438386420243,18.0654055123364));
#48951=CARTESIAN_POINT('Ctrl Pts',(-21.0140471546462,25.5386747640157,18.0649948414849));
#48952=CARTESIAN_POINT('Ctrl Pts',(-21.008465833625,25.5315259117947,18.0644292176641));
#48953=CARTESIAN_POINT('Ctrl Pts',(-21.0069280926294,25.5295515548174,18.0642733096723));
#48954=CARTESIAN_POINT('Ctrl Pts',(-21.0042964858974,25.5261646165937,18.0640063802929));
#48955=CARTESIAN_POINT('Ctrl Pts',(-21.0032014953747,25.5247529173109,18.0638952783044));
#48956=CARTESIAN_POINT('Ctrl Pts',(-21.0010652377073,25.5219940466406,18.0636784584793));
#48957=CARTESIAN_POINT('Ctrl Pts',(-21.0000238669761,25.5206469640978,18.0635727334399));
#48958=CARTESIAN_POINT('Ctrl Pts',(-20.9975342125294,25.5174211499465,18.0633198961075));
#48959=CARTESIAN_POINT('Ctrl Pts',(-20.9960869314369,25.5155416392266,18.0631728558421));
#48960=CARTESIAN_POINT('Ctrl Pts',(-20.9916883177115,25.5098163163054,18.0627257744343));
#48961=CARTESIAN_POINT('Ctrl Pts',(-20.9887435688603,25.5059654188744,18.0624262009121));
#48962=CARTESIAN_POINT('Ctrl Pts',(-20.9602376984585,25.4685129823811,18.0595235176891));
#48963=CARTESIAN_POINT('Ctrl Pts',(-20.935328999713,25.4344168919973,18.0569656526082));
#48964=CARTESIAN_POINT('Ctrl Pts',(-20.8625306830649,25.3305417116966,18.0493912469974));
#48965=CARTESIAN_POINT('Ctrl Pts',(-20.8167095540322,25.2593526855464,18.0444876241887));
#48966=CARTESIAN_POINT('Ctrl Pts',(-20.6797538339028,25.0269466652182,18.0291012268428));
#48967=CARTESIAN_POINT('Ctrl Pts',(-20.5996812653384,24.8596503216587,18.0189194005167));
#48968=CARTESIAN_POINT('Ctrl Pts',(-20.4656278811494,24.5038129862667,17.9974883183425));
#48969=CARTESIAN_POINT('Ctrl Pts',(-20.4135760583289,24.3153866415243,17.9862465660744));
#48970=CARTESIAN_POINT('Ctrl Pts',(-20.3766117710329,24.1108637077341,17.9736185105692));
#48971=CARTESIAN_POINT('Ctrl Pts',(-20.3744157637794,24.0982866407056,17.9728404249817));
#48972=CARTESIAN_POINT('Ctrl Pts',(-20.371522774628,24.0811162365012,17.9717759858902));
#48973=CARTESIAN_POINT('Ctrl Pts',(-20.370760884531,24.0765338317529,17.9714916986339));
#48974=CARTESIAN_POINT('Ctrl Pts',(-20.3694826064335,24.0687415048657,17.9710079057921));
#48975=CARTESIAN_POINT('Ctrl Pts',(-20.3689611617789,24.0655324093624,17.9708085612173));
#48976=CARTESIAN_POINT('Ctrl Pts',(-20.3679632076025,24.0593315022743,17.9704231638871));
#48977=CARTESIAN_POINT('Ctrl Pts',(-20.3674860588078,24.0563397963894,17.9702371317124));
#48978=CARTESIAN_POINT('Ctrl Pts',(-20.3663656842612,24.04925083482,17.9697961005106));
#48979=CARTESIAN_POINT('Ctrl Pts',(-20.3657261491367,24.0451530088802,17.9695409845249));
#48980=CARTESIAN_POINT('Ctrl Pts',(-20.3638693176157,24.0331027146917,17.9687902565791));
#48981=CARTESIAN_POINT('Ctrl Pts',(-20.3626738937624,24.0251469529094,17.9682939510579));
#48982=CARTESIAN_POINT('Ctrl Pts',(-20.3539714746155,23.9657172053102,17.9645814627081));
#48983=CARTESIAN_POINT('Ctrl Pts',(-20.3476823110469,23.9140752378386,17.9613268812482));
#48984=CARTESIAN_POINT('Ctrl Pts',(-20.3309580353865,23.7421659362329,17.950389430731));
#48985=CARTESIAN_POINT('Ctrl Pts',(-20.3260303021233,23.6214776604979,17.9425389830137));
#48986=CARTESIAN_POINT('Ctrl Pts',(-20.330999400122,23.2976302996741,17.9210562763047));
#48987=CARTESIAN_POINT('Ctrl Pts',(-20.3533268589019,23.0952077731006,17.907162137017));
#48988=CARTESIAN_POINT('Ctrl Pts',(-20.4128509865743,22.8079893030754,17.8874748037311));
#48989=CARTESIAN_POINT('Ctrl Pts',(-20.4348403588532,22.7205220738277,17.8814897982656));
#48990=CARTESIAN_POINT('Ctrl Pts',(-20.4607783097774,22.6330460275923,17.8755852394988));
#48991=CARTESIAN_POINT('Ctrl Pts',(-20.4610871922827,22.6320062440132,17.8755150668739));
#48992=CARTESIAN_POINT('Ctrl Pts',(-20.4622631571238,22.6280549314678,17.8752484474633));
#48993=CARTESIAN_POINT('Ctrl Pts',(-20.4631338340247,22.6251444634327,17.875052154516));
#48994=CARTESIAN_POINT('Ctrl Pts',(-20.4644504044655,22.6207660348791,17.8747570030792));
#48995=CARTESIAN_POINT('Ctrl Pts',(-20.4648932305682,22.6192971626541,17.8746580106796));
#48996=CARTESIAN_POINT('Ctrl Pts',(-20.4660956504074,22.6153189684004,17.8743899745764));
#48997=CARTESIAN_POINT('Ctrl Pts',(-20.4668572592981,22.6128102505805,17.8742210199547));
#48998=CARTESIAN_POINT('Ctrl Pts',(-20.4791059581997,22.5726398042475,17.8715168697231));
#48999=CARTESIAN_POINT('Ctrl Pts',(-20.4912799107272,22.5351886048407,17.869012773425));
#49000=CARTESIAN_POINT('Ctrl Pts',(-20.5056968113425,22.493455094257,17.8662488482477));
#49001=CARTESIAN_POINT('Ctrl Pts',(-20.5072657996468,22.488945739395,17.8659505527941));
#49002=CARTESIAN_POINT('Ctrl Pts',(-20.5096421177249,22.4821646677413,17.8655025273824));
#49003=CARTESIAN_POINT('Ctrl Pts',(-20.5104419761549,22.4798903681314,17.8653523567964));
#49004=CARTESIAN_POINT('Ctrl Pts',(-20.5118309609554,22.4759550743302,17.8650926744561));
#49005=CARTESIAN_POINT('Ctrl Pts',(-20.5124188976409,22.47429366618,17.8649830916152));
#49006=CARTESIAN_POINT('Ctrl Pts',(-20.5136460132842,22.4708350715534,17.8647550761786));
#49007=CARTESIAN_POINT('Ctrl Pts',(-20.5142854242678,22.4690379722521,17.864636658223));
#49008=CARTESIAN_POINT('Ctrl Pts',(-20.5155610692619,22.465462756293,17.8644011902862));
#49009=CARTESIAN_POINT('Ctrl Pts',(-20.5161972722307,22.4636846269866,17.8642841382821));
#49010=CARTESIAN_POINT('Ctrl Pts',(-20.5183870341317,22.4575813609004,17.8638825627961));
#49011=CARTESIAN_POINT('Ctrl Pts',(-20.5199482908632,22.4532589622432,17.8635984988085));
#49012=CARTESIAN_POINT('Ctrl Pts',(-20.5327980874533,22.4179205753246,17.861278730786));
#49013=CARTESIAN_POINT('Ctrl Pts',(-20.5445537828858,22.3870748920817,17.8592705235968));
#49014=CARTESIAN_POINT('Ctrl Pts',(-20.5882986686502,22.2773875189196,17.8521706846177));
#49015=CARTESIAN_POINT('Ctrl Pts',(-20.6229352717839,22.1996333647415,17.8472147400845));
#49016=CARTESIAN_POINT('Ctrl Pts',(-20.726317313881,21.9902750655033,17.8338475489804));
#49017=CARTESIAN_POINT('Ctrl Pts',(-20.8011379487566,21.8619063619264,17.8256192126946));
#49018=CARTESIAN_POINT('Ctrl Pts',(-20.9480701938823,21.6456413675228,17.8109895203003));
#49019=CARTESIAN_POINT('Ctrl Pts',(-21.0164715552259,21.5555473988262,17.8046318458246));
#49020=CARTESIAN_POINT('Ctrl Pts',(-21.096159377385,21.4613169320937,17.7975381381758));
#49021=CARTESIAN_POINT('Ctrl Pts',(-21.1028952704148,21.453429319724,17.7969408107351));
#49022=CARTESIAN_POINT('Ctrl Pts',(-21.1883104503336,21.3543819297502,17.7893940243236));
#49023=CARTESIAN_POINT('Ctrl Pts',(-21.2719924370995,21.2676785876644,17.7822893538589));
#49024=CARTESIAN_POINT('Ctrl Pts',(-21.3681564369958,21.1786100137202,17.77431394968));
#49025=CARTESIAN_POINT('Ctrl Pts',(-21.3760269436794,21.1713925762382,17.7736625415275));
#49026=CARTESIAN_POINT('Ctrl Pts',(-21.3871200056261,21.1613210204344,17.7727462205949));
#49027=CARTESIAN_POINT('Ctrl Pts',(-21.3903126898197,21.1584339829715,17.7724827031413));
#49028=CARTESIAN_POINT('Ctrl Pts',(-21.3958593033952,21.1534385283207,17.7720252527943));
#49029=CARTESIAN_POINT('Ctrl Pts',(-21.3982105735938,21.1513271557445,17.7718314448803));
#49030=CARTESIAN_POINT('Ctrl Pts',(-21.403105695686,21.1469444662964,17.7714281820327));
#49031=CARTESIAN_POINT('Ctrl Pts',(-21.4056500535295,21.1446737233623,17.7712187033576));
#49032=CARTESIAN_POINT('Ctrl Pts',(-21.4116433980227,21.1393419565592,17.7707255625168));
#49033=CARTESIAN_POINT('Ctrl Pts',(-21.4150953531824,21.1362842944099,17.7704417599226));
#49034=CARTESIAN_POINT('Ctrl Pts',(-21.4263754784265,21.1263357447834,17.7695151004359));
#49035=CARTESIAN_POINT('Ctrl Pts',(-21.4342304760902,21.1194754988592,17.7688709666022));
#49036=CARTESIAN_POINT('Ctrl Pts',(-21.4526488296631,21.1035465633013,17.7673632110331));
#49037=CARTESIAN_POINT('Ctrl Pts',(-21.4632378645824,21.0945080099667,17.7664983558942));
#49038=CARTESIAN_POINT('Ctrl Pts',(-21.499969069993,21.0635642654826,17.7635049208441));
#49039=CARTESIAN_POINT('Ctrl Pts',(-21.5263994779672,21.0420062360684,17.7613622961688));
#49040=CARTESIAN_POINT('Ctrl Pts',(-21.6470748142823,20.946726347749,17.7516271211319));
#49041=CARTESIAN_POINT('Ctrl Pts',(-21.7450291454913,20.877875897007,17.743848130787));
#49042=CARTESIAN_POINT('Ctrl Pts',(-21.9931448464149,20.723355258478,17.72446837006));
#49043=CARTESIAN_POINT('Ctrl Pts',(-22.146807418224,20.6440062475546,17.7127222203497));
#49044=CARTESIAN_POINT('Ctrl Pts',(-22.4570544134878,20.5141656499843,17.6900179993355));
#49045=CARTESIAN_POINT('Ctrl Pts',(-22.6126521882927,20.4625631410496,17.6790882517949));
#49046=CARTESIAN_POINT('Ctrl Pts',(-22.78075895697,20.4207017756407,17.6681917199969));
#49047=CARTESIAN_POINT('Ctrl Pts',(-22.7900124118544,20.4184410332337,17.6675948125554));
#49048=CARTESIAN_POINT('Ctrl Pts',(-22.8024328705745,20.4154648425978,17.6667976146599));
#49049=CARTESIAN_POINT('Ctrl Pts',(-22.8055910068597,20.4147131339317,17.6665952583028));
#49050=CARTESIAN_POINT('Ctrl Pts',(-22.8105360492825,20.4135439932198,17.6662789543104));
#49051=CARTESIAN_POINT('Ctrl Pts',(-22.8123221740602,20.4131233158326,17.6661648186313));
#49052=CARTESIAN_POINT('Ctrl Pts',(-22.815750243044,20.4123190088805,17.6659459763011));
#49053=CARTESIAN_POINT('Ctrl Pts',(-22.8173921184103,20.4119351448947,17.665841256731));
#49054=CARTESIAN_POINT('Ctrl Pts',(-22.8207816844031,20.4111454827867,17.665625264136));
#49055=CARTESIAN_POINT('Ctrl Pts',(-22.8225294074149,20.4107398567755,17.6655140014579));
#49056=CARTESIAN_POINT('Ctrl Pts',(-22.8264725579163,20.4098281673713,17.665263214239));
#49057=CARTESIAN_POINT('Ctrl Pts',(-22.8286681820471,20.4093229455853,17.6651237384707));
#49058=CARTESIAN_POINT('Ctrl Pts',(-22.8389579928719,20.4069665784305,17.6644708610754));
#49059=CARTESIAN_POINT('Ctrl Pts',(-22.8470588816145,20.4051443938036,17.6639591201188));
#49060=CARTESIAN_POINT('Ctrl Pts',(-22.9378473154056,20.3850910835219,17.658248196046));
#49061=CARTESIAN_POINT('Ctrl Pts',(-23.0212240069743,20.370092335886,17.6532284906616));
#49062=CARTESIAN_POINT('Ctrl Pts',(-23.2409821432845,20.3394439554974,17.6403559575622));
#49063=CARTESIAN_POINT('Ctrl Pts',(-23.3779422902423,20.3291884121211,17.6326858849033));
#49064=CARTESIAN_POINT('Ctrl Pts',(-23.7890621172635,20.324709781385,17.6097100754186));
#49065=CARTESIAN_POINT('Ctrl Pts',(-24.0621947075556,20.3566581345049,17.5944018402668));
#49066=CARTESIAN_POINT('Ctrl Pts',(-24.3451851097992,20.4270308070112,17.5767389446504));
#49067=CARTESIAN_POINT('Ctrl Pts',(-24.3623505723028,20.4314501176043,17.5756608323302));
#49068=CARTESIAN_POINT('Ctrl Pts',(-24.3851933379854,20.4375324369718,17.5742168754131));
#49069=CARTESIAN_POINT('Ctrl Pts',(-24.3909040035974,20.4390698562235,17.5738551125578));
#49070=CARTESIAN_POINT('Ctrl Pts',(-24.3998075174263,20.4414931541219,17.5732898656764));
#49071=CARTESIAN_POINT('Ctrl Pts',(-24.4030033063273,20.4423682581639,17.5730867324745));
#49072=CARTESIAN_POINT('Ctrl Pts',(-24.4091053214691,20.4440492956363,17.572698399261));
#49073=CARTESIAN_POINT('Ctrl Pts',(-24.4120117788116,20.4448543836125,17.5725132269617));
#49074=CARTESIAN_POINT('Ctrl Pts',(-24.4187920126221,20.4467427585085,17.5720807734642));
#49075=CARTESIAN_POINT('Ctrl Pts',(-24.4226648933597,20.4478292186741,17.5718333890171));
#49076=CARTESIAN_POINT('Ctrl Pts',(-24.4337099433469,20.4509500064635,17.5711268231215));
#49077=CARTESIAN_POINT('Ctrl Pts',(-24.4408770663861,20.4530019642048,17.5706670666924));
#49078=CARTESIAN_POINT('Ctrl Pts',(-24.485508997073,20.4659478778045,17.5677960426716));
#49079=CARTESIAN_POINT('Ctrl Pts',(-24.5227791604296,20.4774961803814,17.5653634349968));
#49080=CARTESIAN_POINT('Ctrl Pts',(-24.6327200385592,20.5137623098223,17.5580790782686));
#49081=CARTESIAN_POINT('Ctrl Pts',(-24.7047232213128,20.540401270972,17.5531652266081));
#49082=CARTESIAN_POINT('Ctrl Pts',(-24.8812651598506,20.6129833870207,17.5407538642089));
#49083=CARTESIAN_POINT('Ctrl Pts',(-24.9844390086464,20.6619572188259,17.533170363488));
#49084=CARTESIAN_POINT('Ctrl Pts',(-25.1703845264907,20.7626434619606,17.5189534929859));
#49085=CARTESIAN_POINT('Ctrl Pts',(-25.2538335988041,20.8128444649431,17.5123524518107));
#49086=CARTESIAN_POINT('Ctrl Pts',(-25.4504856959374,20.9436250804692,17.4963805482037));
#49087=CARTESIAN_POINT('Ctrl Pts',(-25.5610119001646,21.027903213778,17.4870416528789));
#49088=CARTESIAN_POINT('Ctrl Pts',(-25.6667271801104,21.1198916013487,17.4779683457058));
#49089=CARTESIAN_POINT('Ctrl Pts',(-25.6676888268072,21.1207293839784,17.4778857978256));
#49090=CARTESIAN_POINT('Ctrl Pts',(-25.6764436462157,21.1283656927844,17.477134176601));
#49091=CARTESIAN_POINT('Ctrl Pts',(-25.6842046508822,21.1352012124491,17.4764671083267));
#49092=CARTESIAN_POINT('Ctrl Pts',(-25.7196162637281,21.1666940401315,17.4734204263193));
#49093=CARTESIAN_POINT('Ctrl Pts',(-25.7468747290597,21.1917908930872,17.4710667313149));
#49094=CARTESIAN_POINT('Ctrl Pts',(-25.7774201488496,21.2209031721931,17.4684256094629));
#49095=CARTESIAN_POINT('Ctrl Pts',(-25.7811360593238,21.2244617585294,17.4681042500663));
#49096=CARTESIAN_POINT('Ctrl Pts',(-25.7866110343877,21.2297301277515,17.4676306938716));
#49097=CARTESIAN_POINT('Ctrl Pts',(-25.7883766709034,21.2314330222551,17.4674779650133));
#49098=CARTESIAN_POINT('Ctrl Pts',(-25.7914968601221,21.2344492191657,17.4672080502637));
#49099=CARTESIAN_POINT('Ctrl Pts',(-25.7928522047507,21.2357616960006,17.4670907996523));
#49100=CARTESIAN_POINT('Ctrl Pts',(-25.7956778556885,21.2385027875506,17.4668463430857));
#49101=CARTESIAN_POINT('Ctrl Pts',(-25.7971479485206,21.2399316121933,17.4667191544568));
#49102=CARTESIAN_POINT('Ctrl Pts',(-25.8001270856233,21.2428326525475,17.4664613926171));
#49103=CARTESIAN_POINT('Ctrl Pts',(-25.8016360508921,21.2443049484555,17.466330825827));
#49104=CARTESIAN_POINT('Ctrl Pts',(-25.8053486611656,21.2479344565997,17.466009561327));
#49105=CARTESIAN_POINT('Ctrl Pts',(-25.807550662358,21.2500933586037,17.4658189956201));
#49106=CARTESIAN_POINT('Ctrl Pts',(-25.8279328235101,21.2701340421791,17.4640548638619));
#49107=CARTESIAN_POINT('Ctrl Pts',(-25.8459039194147,21.2882285172376,17.462497808267));
#49108=CARTESIAN_POINT('Ctrl Pts',(-25.939113719498,21.3843333788518,17.4544008172419));
#49109=CARTESIAN_POINT('Ctrl Pts',(-26.0106042154937,21.4658969714548,17.448116204365));
#49110=CARTESIAN_POINT('Ctrl Pts',(-26.1014921883155,21.5807994355283,17.4397792577676));
#49111=CARTESIAN_POINT('Ctrl Pts',(-26.1245982785293,21.6110997879473,17.4376261707485));
#49112=CARTESIAN_POINT('Ctrl Pts',(-26.1715372244686,21.6749716422224,17.4331656572905));
#49113=CARTESIAN_POINT('Ctrl Pts',(-26.1952749820359,21.7086043135896,17.430860134811));
#49114=CARTESIAN_POINT('Ctrl Pts',(-26.2768363928449,21.8289951229054,17.4227274554058));
#49115=CARTESIAN_POINT('Ctrl Pts',(-26.3310873937282,21.9180933376937,17.4169219001377));
#49116=CARTESIAN_POINT('Ctrl Pts',(-26.4720715730959,22.1771368796409,17.4002825862503));
#49117=CARTESIAN_POINT('Ctrl Pts',(-26.5481633465448,22.3523429349545,17.3892800956125));
#49118=CARTESIAN_POINT('Ctrl Pts',(-26.6123038599256,22.5452060091682,17.3769295735889));
#49119=CARTESIAN_POINT('Ctrl Pts',(-26.6162162774602,22.5572051251165,17.376160367814));
#49120=CARTESIAN_POINT('Ctrl Pts',(-26.6214652804226,22.5736301968753,17.3751062318943));
#49121=CARTESIAN_POINT('Ctrl Pts',(-26.6228630096105,22.5780366176833,17.3748233166947));
#49122=CARTESIAN_POINT('Ctrl Pts',(-26.6252257362638,22.5855412361682,17.3743412749088));
#49123=CARTESIAN_POINT('Ctrl Pts',(-26.626195547031,22.5886379213526,17.3741423068719));
#49124=CARTESIAN_POINT('Ctrl Pts',(-26.628062267765,22.5946302317464,17.3737571718536));
#49125=CARTESIAN_POINT('Ctrl Pts',(-26.6289597727228,22.5975256686586,17.3735710247027));
#49126=CARTESIAN_POINT('Ctrl Pts',(-26.6310797574491,22.6043992198992,17.3731289975566));
#49127=CARTESIAN_POINT('Ctrl Pts',(-26.6322986170293,22.6083784371368,17.3728729990347));
#49128=CARTESIAN_POINT('Ctrl Pts',(-26.6358710180386,22.6201224597623,17.3721171550486));
#49129=CARTESIAN_POINT('Ctrl Pts',(-26.6382029348119,22.6278937620511,17.3716166015833));
#49130=CARTESIAN_POINT('Ctrl Pts',(-26.6434009856207,22.6454573571574,17.3704844005209));
#49131=CARTESIAN_POINT('Ctrl Pts',(-26.6462500027706,22.6552545869331,17.3698521976048));
#49132=CARTESIAN_POINT('Ctrl Pts',(-26.6552224627898,22.6866647231777,17.3678231934226));
#49133=CARTESIAN_POINT('Ctrl Pts',(-26.6611663707847,22.708327819782,17.3664205673953));
#49134=CARTESIAN_POINT('Ctrl Pts',(-26.7375947597152,22.9987430515741,17.3475705571188));
#49135=CARTESIAN_POINT('Ctrl Pts',(-26.7732452352441,23.275386012713,17.3289302935924));
#49136=CARTESIAN_POINT('Ctrl Pts',(-26.7730012882014,23.5530835971147,17.3101346383694));
#49137=CARTESIAN_POINT('Ctrl Pts',(-22.0738786772418,26.4178312615861,16.9038400528878));
#49138=CARTESIAN_POINT('Ctrl Pts',(-22.8848601554831,26.8257766505266,16.9600102888025));
#49139=CARTESIAN_POINT('Ctrl Pts',(-25.0566874879774,26.9584629849414,17.0824761618423));
#49140=CARTESIAN_POINT('Ctrl Pts',(-26.6594709648069,25.0501006738249,17.218120627304));
#49141=CARTESIAN_POINT('Ctrl Pts',(-26.7760869353403,23.7663575325862,17.2975948568509));
#49142=CARTESIAN_POINT('Ctrl Pts',(-26.7741131953272,23.5531281751,17.3107734492729));
#49143=CARTESIAN_POINT('Ctrl Pts',(-22.075036069343,26.4155368023571,16.6585071611381));
#49144=CARTESIAN_POINT('Ctrl Pts',(-22.203393445971,26.4816227111811,16.6682250130379));
#49145=CARTESIAN_POINT('Ctrl Pts',(-22.3360903487222,26.5390313531522,16.6778097090526));
#49146=CARTESIAN_POINT('Ctrl Pts',(-22.4821328897951,26.5908689608885,16.6875644177171));
#49147=CARTESIAN_POINT('Ctrl Pts',(-22.4920464967325,26.5943333180319,16.6882227385446));
#49148=CARTESIAN_POINT('Ctrl Pts',(-22.505044801427,26.5988044646475,16.6890807117283));
#49149=CARTESIAN_POINT('Ctrl Pts',(-22.5081141880536,26.5998550894481,16.6892829336088));
#49150=CARTESIAN_POINT('Ctrl Pts',(-22.5131144720326,26.6015582131558,16.6896117489145));
#49151=CARTESIAN_POINT('Ctrl Pts',(-22.5150444014581,26.6022135150076,16.6897385093671));
#49152=CARTESIAN_POINT('Ctrl Pts',(-22.5187661564798,26.6034732895566,16.6899826677612));
#49153=CARTESIAN_POINT('Ctrl Pts',(-22.520557887755,26.6040780143883,16.6901000803396));
#49154=CARTESIAN_POINT('Ctrl Pts',(-22.5247005673667,26.6054721442679,16.6903712515863));
#49155=CARTESIAN_POINT('Ctrl Pts',(-22.5270519018028,26.6062604151395,16.6905249423718));
#49156=CARTESIAN_POINT('Ctrl Pts',(-22.5344107843417,26.6087179915011,16.6910052530175));
#49157=CARTESIAN_POINT('Ctrl Pts',(-22.5394215577847,26.6103777199208,16.691331305525));
#49158=CARTESIAN_POINT('Ctrl Pts',(-22.5829446231347,26.6246753852068,16.6941548916166));
#49159=CARTESIAN_POINT('Ctrl Pts',(-22.6216902456656,26.6365987414654,16.6966110253976));
#49160=CARTESIAN_POINT('Ctrl Pts',(-22.6673420324709,26.6497097505165,16.699449181005));
#49161=CARTESIAN_POINT('Ctrl Pts',(-22.6740376593446,26.6516092509473,16.6998640504444));
#49162=CARTESIAN_POINT('Ctrl Pts',(-22.6844324151706,26.6545218172238,16.7005060350336));
#49163=CARTESIAN_POINT('Ctrl Pts',(-22.6881272478295,26.6555499838628,16.7007338211858));
#49164=CARTESIAN_POINT('Ctrl Pts',(-22.6976219044861,26.658173824116,16.7013181385336));
#49165=CARTESIAN_POINT('Ctrl Pts',(-22.703424399568,26.6597598659795,16.7016742503375));
#49166=CARTESIAN_POINT('Ctrl Pts',(-22.709830556491,26.6614916500195,16.7020663600588));
#49167=CARTESIAN_POINT('Ctrl Pts',(-22.7104298192741,26.6616534636702,16.7021030297633));
#49168=CARTESIAN_POINT('Ctrl Pts',(-22.7171976109482,26.6634788131658,16.7025170461531));
#49169=CARTESIAN_POINT('Ctrl Pts',(-22.7233710713558,26.6651241875254,16.7028936354194));
#49170=CARTESIAN_POINT('Ctrl Pts',(-22.7420979277533,26.6700557439983,16.7040328723909));
#49171=CARTESIAN_POINT('Ctrl Pts',(-22.7546664385469,26.6732845079295,16.7047932191728));
#49172=CARTESIAN_POINT('Ctrl Pts',(-22.9367178240878,26.7188819144376,16.7157497062546));
#49173=CARTESIAN_POINT('Ctrl Pts',(-23.1093662734825,26.7474804626039,16.7254405211916));
#49174=CARTESIAN_POINT('Ctrl Pts',(-23.4312041113768,26.7742118812468,16.7434931444036));
#49175=CARTESIAN_POINT('Ctrl Pts',(-23.5795773170386,26.7762751801357,16.7518113925727));
#49176=CARTESIAN_POINT('Ctrl Pts',(-23.8272576200464,26.7626279937179,16.7661874766666));
#49177=CARTESIAN_POINT('Ctrl Pts',(-23.9266400805841,26.7525044439856,16.7720868025484));
#49178=CARTESIAN_POINT('Ctrl Pts',(-24.0370510660604,26.7360466014992,16.7788495708175));
#49179=CARTESIAN_POINT('Ctrl Pts',(-24.0487067366648,26.7342437484007,16.7795660786807));
#49180=CARTESIAN_POINT('Ctrl Pts',(-24.0666223172816,26.7313718523986,16.7806714832075));
#49181=CARTESIAN_POINT('Ctrl Pts',(-24.0728894852024,26.7303482066616,16.7810589418499));
#49182=CARTESIAN_POINT('Ctrl Pts',(-24.0832266041961,26.7286284140417,16.7816993053104));
#49183=CARTESIAN_POINT('Ctrl Pts',(-24.0872983355942,26.7279429533228,16.7819518703907));
#49184=CARTESIAN_POINT('Ctrl Pts',(-24.0951853648166,26.7265996095837,16.7824417377792));
#49185=CARTESIAN_POINT('Ctrl Pts',(-24.0990008183009,26.7259426723673,16.7826790096245));
#49186=CARTESIAN_POINT('Ctrl Pts',(-24.1059027251022,26.7247415059167,16.7831087510774));
#49187=CARTESIAN_POINT('Ctrl Pts',(-24.1089895905496,26.7241996459114,16.7833011449433));
#49188=CARTESIAN_POINT('Ctrl Pts',(-24.1154124768224,26.7230625295216,16.7837018650197));
#49189=CARTESIAN_POINT('Ctrl Pts',(-24.1187483573803,26.7224665128009,16.7839102152615));
#49190=CARTESIAN_POINT('Ctrl Pts',(-24.128270500228,26.7207497035339,16.7845055936798));
#49191=CARTESIAN_POINT('Ctrl Pts',(-24.1344544059581,26.7196160731329,16.7848930311963));
#49192=CARTESIAN_POINT('Ctrl Pts',(-24.1609506111018,26.7146786214358,16.7865564827146));
#49193=CARTESIAN_POINT('Ctrl Pts',(-24.1812290262424,26.7106976353016,16.7878381460078));
#49194=CARTESIAN_POINT('Ctrl Pts',(-24.5386775994443,26.6369473353225,16.81058556711));
#49195=CARTESIAN_POINT('Ctrl Pts',(-24.862495103852,26.5137914170664,16.8340027861256));
#49196=CARTESIAN_POINT('Ctrl Pts',(-25.2916157992142,26.2662521184879,16.8673558209928));
#49197=CARTESIAN_POINT('Ctrl Pts',(-25.4171817976899,26.181523656607,16.8773946094422));
#49198=CARTESIAN_POINT('Ctrl Pts',(-25.541166820741,26.0845010108741,16.8872593990503));
#49199=CARTESIAN_POINT('Ctrl Pts',(-25.5459786129662,26.0807134522688,16.8876421552228));
#49200=CARTESIAN_POINT('Ctrl Pts',(-25.5528364703138,26.0752836233906,16.8881875004019));
#49201=CARTESIAN_POINT('Ctrl Pts',(-25.5548913327615,26.0736525639173,16.8883508841691));
#49202=CARTESIAN_POINT('Ctrl Pts',(-25.5584371401185,26.0708309933106,16.8886327737449));
#49203=CARTESIAN_POINT('Ctrl Pts',(-25.5599290215553,26.0696416657602,16.8887513650174));
#49204=CARTESIAN_POINT('Ctrl Pts',(-25.5627966392919,26.0673514336195,16.8889792898488));
#49205=CARTESIAN_POINT('Ctrl Pts',(-25.5641725262492,26.0662507277723,16.8890886374592));
#49206=CARTESIAN_POINT('Ctrl Pts',(-25.5674274998922,26.0636423769247,16.889347299826));
#49207=CARTESIAN_POINT('Ctrl Pts',(-25.5693058033178,26.0621337495998,16.8894965434142));
#49208=CARTESIAN_POINT('Ctrl Pts',(-25.5748960718123,26.0576334016326,16.8899406758766));
#49209=CARTESIAN_POINT('Ctrl Pts',(-25.5786031128428,26.0546355319797,16.8902351233657));
#49210=CARTESIAN_POINT('Ctrl Pts',(-25.6127034566538,26.0269333342815,16.8929432098302));
#49211=CARTESIAN_POINT('Ctrl Pts',(-25.6426523481806,26.001683738597,16.8953181015725));
#49212=CARTESIAN_POINT('Ctrl Pts',(-25.6762951083699,25.9722539918827,16.8979917156576));
#49213=CARTESIAN_POINT('Ctrl Pts',(-25.6804457815069,25.9686042079968,16.8983216754071));
#49214=CARTESIAN_POINT('Ctrl Pts',(-25.9066958234451,25.7686228282329,16.9163144806829));
#49215=CARTESIAN_POINT('Ctrl Pts',(-26.100684783078,25.5425722949492,16.9322195447708));
#49216=CARTESIAN_POINT('Ctrl Pts',(-26.326384589936,25.1915337933888,16.9559171470612));
#49217=CARTESIAN_POINT('Ctrl Pts',(-26.3859499603648,25.0863284095013,16.9628952520117));
#49218=CARTESIAN_POINT('Ctrl Pts',(-26.4625494529594,24.9313241960944,16.9731825732099));
#49219=CARTESIAN_POINT('Ctrl Pts',(-26.4844955586872,24.8840627428085,16.9763192104321));
#49220=CARTESIAN_POINT('Ctrl Pts',(-26.508483182764,24.8289445154798,16.9799845001277));
#49221=CARTESIAN_POINT('Ctrl Pts',(-26.5116534261184,24.8215851062008,16.9804740331189));
#49222=CARTESIAN_POINT('Ctrl Pts',(-26.5164202373603,24.8104048445706,16.9812179636424));
#49223=CARTESIAN_POINT('Ctrl Pts',(-26.51803695876,24.8065925748335,16.9814716732277));
#49224=CARTESIAN_POINT('Ctrl Pts',(-26.5208234869384,24.7999864778937,16.9819113919028));
#49225=CARTESIAN_POINT('Ctrl Pts',(-26.5219967136411,24.7971940914264,16.9820972842513));
#49226=CARTESIAN_POINT('Ctrl Pts',(-26.5244223507065,24.7913979869309,16.9824831890764));
#49227=CARTESIAN_POINT('Ctrl Pts',(-26.5256741508472,24.7883940185744,16.9826832220561));
#49228=CARTESIAN_POINT('Ctrl Pts',(-26.5290746197132,24.7801989106864,16.9832290118291));
#49229=CARTESIAN_POINT('Ctrl Pts',(-26.5312142598612,24.7750040582621,16.9835750747256));
#49230=CARTESIAN_POINT('Ctrl Pts',(-26.539257206653,24.7553305771579,16.9848860074838));
#49231=CARTESIAN_POINT('Ctrl Pts',(-26.545068626038,24.7408148315268,16.9858539830078));
#49232=CARTESIAN_POINT('Ctrl Pts',(-26.6374030443426,24.5052279045971,17.0015773089992));
#49233=CARTESIAN_POINT('Ctrl Pts',(-26.6993261250103,24.2753510642032,17.0171925038953));
#49234=CARTESIAN_POINT('Ctrl Pts',(-26.7605361386873,23.8779128292599,17.0443129103014));
#49235=CARTESIAN_POINT('Ctrl Pts',(-26.7730913015098,23.7133304407264,17.0555543233618));
#49236=CARTESIAN_POINT('Ctrl Pts',(-26.7729828646908,23.5130563265239,17.0688456133548));
#49237=CARTESIAN_POINT('Ctrl Pts',(-26.7723787071759,23.4776066007037,17.0711828109468));
#49238=CARTESIAN_POINT('Ctrl Pts',(-26.7709592611565,23.4353049460033,17.0739481510603));
#49239=CARTESIAN_POINT('Ctrl Pts',(-26.7707068361009,23.4284376748799,17.0743963336792));
#49240=CARTESIAN_POINT('Ctrl Pts',(-26.7704043778455,23.42086882187,17.0748894476697));
#49241=CARTESIAN_POINT('Ctrl Pts',(-26.7703760798166,23.4201664391476,17.0749352000718));
#49242=CARTESIAN_POINT('Ctrl Pts',(-26.7700668842762,23.4125538487842,17.0754309869418));
#49243=CARTESIAN_POINT('Ctrl Pts',(-26.7697639713918,23.4056444974206,17.0758801834118));
#49244=CARTESIAN_POINT('Ctrl Pts',(-26.7692581165855,23.394896877251,17.076577634149));
#49245=CARTESIAN_POINT('Ctrl Pts',(-26.7690705474334,23.3910579439773,17.0768265013508));
#49246=CARTESIAN_POINT('Ctrl Pts',(-26.7686766104764,23.3832807867885,17.0773301446878));
#49247=CARTESIAN_POINT('Ctrl Pts',(-26.7684698806755,23.3793425860954,17.077584905576));
#49248=CARTESIAN_POINT('Ctrl Pts',(-26.768181083878,23.374027396544,17.0779283645859));
#49249=CARTESIAN_POINT('Ctrl Pts',(-26.7681053617023,23.3726500833997,17.0780173300082));
#49250=CARTESIAN_POINT('Ctrl Pts',(-26.7677543190166,23.3663388832228,17.0784248336488));
#49251=CARTESIAN_POINT('Ctrl Pts',(-26.767468533422,23.3614055556319,17.0787429261173));
#49252=CARTESIAN_POINT('Ctrl Pts',(-26.7649726004756,23.3199707948098,17.0814107300028));
#49253=CARTESIAN_POINT('Ctrl Pts',(-26.7621525620342,23.2835068149709,17.0837334805551));
#49254=CARTESIAN_POINT('Ctrl Pts',(-26.7582725994224,23.2424430798982,17.0863150844098));
#49255=CARTESIAN_POINT('Ctrl Pts',(-26.7578227522447,23.2377902228413,17.0866071055414));
#49256=CARTESIAN_POINT('Ctrl Pts',(-26.7571280613425,23.2307645195658,17.0870472847863));
#49257=CARTESIAN_POINT('Ctrl Pts',(-26.7568907065372,23.2283909647421,17.0871958623471));
#49258=CARTESIAN_POINT('Ctrl Pts',(-26.7564740594076,23.224270690389,17.0874535475621));
#49259=CARTESIAN_POINT('Ctrl Pts',(-26.7562959748801,23.2225238541687,17.0875627237091));
#49260=CARTESIAN_POINT('Ctrl Pts',(-26.7559209092336,23.2188743873842,17.0877906605835));
#49261=CARTESIAN_POINT('Ctrl Pts',(-26.7557236620015,23.216971788072,17.0879094055793));
#49262=CARTESIAN_POINT('Ctrl Pts',(-26.7552490795484,23.2124334756641,17.0881924459315));
#49263=CARTESIAN_POINT('Ctrl Pts',(-26.7549701859103,23.209797919079,17.0883566526268));
#49264=CARTESIAN_POINT('Ctrl Pts',(-26.7540197228722,23.2009206595064,17.0889091987368));
#49265=CARTESIAN_POINT('Ctrl Pts',(-26.753333161597,23.1946805247733,17.0892966931835));
#49266=CARTESIAN_POINT('Ctrl Pts',(-26.7395253105707,23.0724674594848,17.0968686484191));
#49267=CARTESIAN_POINT('Ctrl Pts',(-26.7201300397475,22.9572744117898,17.1037043248199));
#49268=CARTESIAN_POINT('Ctrl Pts',(-26.6211092682994,22.5168192196363,17.1295373365877));
#49269=CARTESIAN_POINT('Ctrl Pts',(-26.4972804191143,22.2037046951988,17.147481641968));
#49270=CARTESIAN_POINT('Ctrl Pts',(-26.3253791337552,21.9117145515364,17.1675571083032));
#49271=CARTESIAN_POINT('Ctrl Pts',(-26.323292500491,21.9081856325931,17.1678002325554));
#49272=CARTESIAN_POINT('Ctrl Pts',(-26.3194914566779,21.9017852060803,17.1682420995423));
#49273=CARTESIAN_POINT('Ctrl Pts',(-26.3177792969328,21.8989123635793,17.1684407664592));
#49274=CARTESIAN_POINT('Ctrl Pts',(-26.3145647813033,21.8935377508397,17.1688130694243));
#49275=CARTESIAN_POINT('Ctrl Pts',(-26.313063492128,21.8910353442028,17.1689866691995));
#49276=CARTESIAN_POINT('Ctrl Pts',(-26.307967515529,21.882567267175,17.1695749997308));
#49277=CARTESIAN_POINT('Ctrl Pts',(-26.3043569053319,21.8766112405062,17.1699902728998));
#49278=CARTESIAN_POINT('Ctrl Pts',(-26.2992160838801,21.8681926764866,17.1705793531379));
#49279=CARTESIAN_POINT('Ctrl Pts',(-26.2977017969995,21.8657204001393,17.1707526068798));
#49280=CARTESIAN_POINT('Ctrl Pts',(-26.2930747891287,21.8581890251485,17.1712811886394));
#49281=CARTESIAN_POINT('Ctrl Pts',(-26.289951427309,21.8531365053921,17.171636887715));
#49282=CARTESIAN_POINT('Ctrl Pts',(-26.2833419111319,21.8425103893565,17.1723872980491));
#49283=CARTESIAN_POINT('Ctrl Pts',(-26.2798526387113,21.8369387730597,17.1727821184688));
#49284=CARTESIAN_POINT('Ctrl Pts',(-26.2616963376852,21.808143316208,17.1748297484953));
#49285=CARTESIAN_POINT('Ctrl Pts',(-26.246750231627,21.7850975486398,17.1764925275838));
#49286=CARTESIAN_POINT('Ctrl Pts',(-26.2266589156883,21.7549690061379,17.1786993593265));
#49287=CARTESIAN_POINT('Ctrl Pts',(-26.2217765431543,21.7477116796648,17.1792334985503));
#49288=CARTESIAN_POINT('Ctrl Pts',(-26.2144550102438,21.7369237889745,17.1800313489825));
#49289=CARTESIAN_POINT('Ctrl Pts',(-26.2120382164435,21.7333780329837,17.1802942111124));
#49290=CARTESIAN_POINT('Ctrl Pts',(-26.2077146842624,21.7270619820367,17.1807635685288));
#49291=CARTESIAN_POINT('Ctrl Pts',(-26.2058106740334,21.7242898198042,17.1809699597234));
#49292=CARTESIAN_POINT('Ctrl Pts',(-26.2017869782356,21.7184510855031,17.1814054800818));
#49293=CARTESIAN_POINT('Ctrl Pts',(-26.1996663054006,21.7153852027105,17.1816346467471));
#49294=CARTESIAN_POINT('Ctrl Pts',(-26.1940500130129,21.7072956964706,17.1822405835769));
#49295=CARTESIAN_POINT('Ctrl Pts',(-26.1905454070001,21.7022783569541,17.1826176974889));
#49296=CARTESIAN_POINT('Ctrl Pts',(-26.1746179528444,21.6796137497295,17.1843271201599));
#49297=CARTESIAN_POINT('Ctrl Pts',(-26.1620325553196,21.6620818857996,17.1856656718201));
#49298=CARTESIAN_POINT('Ctrl Pts',(-26.0684510537562,21.5344457446201,17.1955325137109));
#49299=CARTESIAN_POINT('Ctrl Pts',(-25.980710036165,21.4294818518882,17.2043273003613));
#49300=CARTESIAN_POINT('Ctrl Pts',(-25.778350100587,21.2165025674078,17.2237051598486));
#49301=CARTESIAN_POINT('Ctrl Pts',(-25.6619391534872,21.1106664166353,17.2343363776029));
#49302=CARTESIAN_POINT('Ctrl Pts',(-25.3865767566106,20.8948459038679,17.2580151878347));
#49303=CARTESIAN_POINT('Ctrl Pts',(-25.2244872148298,20.789776487479,17.2710215678252));
#49304=CARTESIAN_POINT('Ctrl Pts',(-25.0433904789264,20.6942414257646,17.2839302350354));
#49305=CARTESIAN_POINT('Ctrl Pts',(-25.0327898358473,20.6887243527105,17.2846801895551));
#49306=CARTESIAN_POINT('Ctrl Pts',(-25.0189986643707,20.6816439880012,17.2856482930714));
#49307=CARTESIAN_POINT('Ctrl Pts',(-25.0158360768246,20.6800269217928,17.2858697843376));
#49308=CARTESIAN_POINT('Ctrl Pts',(-25.0109806482107,20.6775544045836,17.2862090381496));
#49309=CARTESIAN_POINT('Ctrl Pts',(-25.0092897277077,20.6766952205242,17.2863270368157));
#49310=CARTESIAN_POINT('Ctrl Pts',(-25.0059512169783,20.6750025757172,17.2865597175737));
#49311=CARTESIAN_POINT('Ctrl Pts',(-25.0043036777437,20.6741690425738,17.2866744036544));
#49312=CARTESIAN_POINT('Ctrl Pts',(-25.0006694538914,20.6723343147293,17.2869270741811));
#49313=CARTESIAN_POINT('Ctrl Pts',(-24.9986824535812,20.6713337636168,17.2870650174024));
#49314=CARTESIAN_POINT('Ctrl Pts',(-24.9930007261856,20.6684801092578,17.2874588820946));
#49315=CARTESIAN_POINT('Ctrl Pts',(-24.9893034506443,20.6666320468618,17.2877144854428));
#49316=CARTESIAN_POINT('Ctrl Pts',(-24.9809648049732,20.6624840532316,17.2882894150135));
#49317=CARTESIAN_POINT('Ctrl Pts',(-24.9763214115896,20.6601881821031,17.2886084899302));
#49318=CARTESIAN_POINT('Ctrl Pts',(-24.8179767615122,20.5823710724214,17.2994533631232));
#49319=CARTESIAN_POINT('Ctrl Pts',(-24.6584790065058,20.5191969735644,17.3092320109603));
#49320=CARTESIAN_POINT('Ctrl Pts',(-24.2365863909219,20.3898821146604,17.3340416157873));
#49321=CARTESIAN_POINT('Ctrl Pts',(-23.9695862302417,20.3435179636237,17.3488414563069));
#49322=CARTESIAN_POINT('Ctrl Pts',(-23.6907261721221,20.3305522852027,17.3653221725283));
#49323=CARTESIAN_POINT('Ctrl Pts',(-23.6815171031978,20.3301636927435,17.3658674361528));
#49324=CARTESIAN_POINT('Ctrl Pts',(-23.6137344471982,20.3275947420582,17.3698885249926));
#49325=CARTESIAN_POINT('Ctrl Pts',(-23.5551158161485,20.3269733231394,17.3734086717156));
#49326=CARTESIAN_POINT('Ctrl Pts',(-23.4875134029064,20.3281007001469,17.3775281509878));
#49327=CARTESIAN_POINT('Ctrl Pts',(-23.4785119898456,20.3282885474309,17.3780778863707));
#49328=CARTESIAN_POINT('Ctrl Pts',(-23.4652173706675,20.3286217279744,17.3788916533468));
#49329=CARTESIAN_POINT('Ctrl Pts',(-23.4609234239531,20.3287379307163,17.3791547699035));
#49330=CARTESIAN_POINT('Ctrl Pts',(-23.4532584100905,20.3289606979213,17.3796249624165));
#49331=CARTESIAN_POINT('Ctrl Pts',(-23.4498872475059,20.3290639703787,17.3798319346804));
#49332=CARTESIAN_POINT('Ctrl Pts',(-23.4428300935526,20.3292912490605,17.3802655793531));
#49333=CARTESIAN_POINT('Ctrl Pts',(-23.4391441424881,20.3294162908851,17.3804922840004));
#49334=CARTESIAN_POINT('Ctrl Pts',(-23.4295197645335,20.3297593281706,17.3810847897676));
#49335=CARTESIAN_POINT('Ctrl Pts',(-23.4235817316131,20.3299874210771,17.3814509076436));
#49336=CARTESIAN_POINT('Ctrl Pts',(-23.3994972087006,20.3309792792366,17.3829381481657));
#49337=CARTESIAN_POINT('Ctrl Pts',(-23.381356971284,20.3318800067527,17.3840635661922));
#49338=CARTESIAN_POINT('Ctrl Pts',(-23.257137183239,20.3391010649941,17.3918071169068));
#49339=CARTESIAN_POINT('Ctrl Pts',(-23.1514300689748,20.3505108633688,17.3985847757824));
#49340=CARTESIAN_POINT('Ctrl Pts',(-22.8168345509397,20.4034640762691,17.420660991824));
#49341=CARTESIAN_POINT('Ctrl Pts',(-22.5918082394972,20.4645533608228,17.4365075035587));
#49342=CARTESIAN_POINT('Ctrl Pts',(-22.2708968236224,20.5901936211964,17.4597425212286));
#49343=CARTESIAN_POINT('Ctrl Pts',(-22.1686432731656,20.6365161302416,17.4672362312153));
#49344=CARTESIAN_POINT('Ctrl Pts',(-22.0679029185401,20.6886518029306,17.4745803501861));
#49345=CARTESIAN_POINT('Ctrl Pts',(-22.0667997029764,20.6892235539561,17.4746607710712));
#49346=CARTESIAN_POINT('Ctrl Pts',(-22.0559681363789,20.694845056538,17.4754503051783));
#49347=CARTESIAN_POINT('Ctrl Pts',(-22.0462651414434,20.6999438396518,17.4761571600226));
#49348=CARTESIAN_POINT('Ctrl Pts',(-22.0044216299058,20.7222051608535,17.4792030300762));
#49349=CARTESIAN_POINT('Ctrl Pts',(-21.9725458417482,20.7398634145975,17.4815172131766));
#49350=CARTESIAN_POINT('Ctrl Pts',(-21.9369290421668,20.7603911219688,17.4840901801243));
#49351=CARTESIAN_POINT('Ctrl Pts',(-21.9328883697418,20.7627316733649,17.4843818907656));
#49352=CARTESIAN_POINT('Ctrl Pts',(-21.9267923649877,20.7662804891594,17.4848216811508));
#49353=CARTESIAN_POINT('Ctrl Pts',(-21.9247332848705,20.7674822528544,17.4849701793072));
#49354=CARTESIAN_POINT('Ctrl Pts',(-21.9211603013957,20.7695729115873,17.4852277649209));
#49355=CARTESIAN_POINT('Ctrl Pts',(-21.9196457910503,20.7704607585756,17.4853369207428));
#49356=CARTESIAN_POINT('Ctrl Pts',(-21.9164824107231,20.7723186926438,17.4855648539608));
#49357=CARTESIAN_POINT('Ctrl Pts',(-21.914833680252,20.7732890096639,17.4856836155706));
#49358=CARTESIAN_POINT('Ctrl Pts',(-21.9109476610757,20.7755806853145,17.4859634523854));
#49359=CARTESIAN_POINT('Ctrl Pts',(-21.9087110981058,20.776903286494,17.4861244461464));
#49360=CARTESIAN_POINT('Ctrl Pts',(-21.9012944167472,20.7813012881344,17.4866581152386));
#49361=CARTESIAN_POINT('Ctrl Pts',(-21.896121282052,20.784388532072,17.4870300196998));
#49362=CARTESIAN_POINT('Ctrl Pts',(-21.8838865410553,20.7917366322493,17.487908885957));
#49363=CARTESIAN_POINT('Ctrl Pts',(-21.8768325343594,20.796010149805,17.4884150402478));
#49364=CARTESIAN_POINT('Ctrl Pts',(-21.6175917980384,20.954429164875,17.5069989100566));
#49365=CARTESIAN_POINT('Ctrl Pts',(-21.3877394375596,21.1425394854986,17.5229462899249));
#49366=CARTESIAN_POINT('Ctrl Pts',(-21.0493874336616,21.5075561421739,17.5509583986936));
#49367=CARTESIAN_POINT('Ctrl Pts',(-20.926301710661,21.668285936696,17.5625739832365));
#49368=CARTESIAN_POINT('Ctrl Pts',(-20.8123906606256,21.8501382378066,17.5756134444197));
#49369=CARTESIAN_POINT('Ctrl Pts',(-20.8057664954906,21.8608524525673,17.5763811793827));
#49370=CARTESIAN_POINT('Ctrl Pts',(-20.7967993612295,21.875548218203,17.5774336168578));
#49371=CARTESIAN_POINT('Ctrl Pts',(-20.7944018259461,21.8794964792332,17.5777163128799));
#49372=CARTESIAN_POINT('Ctrl Pts',(-20.7903349381036,21.8862264010545,17.5781980819669));
#49373=CARTESIAN_POINT('Ctrl Pts',(-20.7886612769601,21.8890054614112,17.5783969968857));
#49374=CARTESIAN_POINT('Ctrl Pts',(-20.7854315929023,21.894386615916,17.5787821095743));
#49375=CARTESIAN_POINT('Ctrl Pts',(-20.7838750398147,21.8969883885692,17.57896828764));
#49376=CARTESIAN_POINT('Ctrl Pts',(-20.7801891821573,21.9031690655086,17.579410513511));
#49377=CARTESIAN_POINT('Ctrl Pts',(-20.7780631424843,21.9067499016012,17.5796666801297));
#49378=CARTESIAN_POINT('Ctrl Pts',(-20.7718090513784,21.9173301752278,17.5804234587369));
#49379=CARTESIAN_POINT('Ctrl Pts',(-20.7677005487745,21.9243410777805,17.5809247813381));
#49380=CARTESIAN_POINT('Ctrl Pts',(-20.7379670817228,21.9755221561321,17.5845835748412));
#49381=CARTESIAN_POINT('Ctrl Pts',(-20.7133698857937,22.0202781601466,17.5877779976963));
#49382=CARTESIAN_POINT('Ctrl Pts',(-20.6355792757842,22.1701531646646,17.598467039943));
#49383=CARTESIAN_POINT('Ctrl Pts',(-20.5870905309683,22.2775939014891,17.6061208766361));
#49384=CARTESIAN_POINT('Ctrl Pts',(-20.4617147282357,22.601666681875,17.6291428712486));
#49385=CARTESIAN_POINT('Ctrl Pts',(-20.4019826547138,22.8241220955053,17.6449122698399));
#49386=CARTESIAN_POINT('Ctrl Pts',(-20.3606170445335,23.0879336879652,17.6627235615881));
#49387=CARTESIAN_POINT('Ctrl Pts',(-20.3554718989437,23.1249407187237,17.6652006099861));
#49388=CARTESIAN_POINT('Ctrl Pts',(-20.3498470207476,23.1712944562916,17.6682703313811));
#49389=CARTESIAN_POINT('Ctrl Pts',(-20.3487630393551,23.1805638907707,17.6688825457223));
#49390=CARTESIAN_POINT('Ctrl Pts',(-20.3470430970871,23.1958467708995,17.6698890888089));
#49391=CARTESIAN_POINT('Ctrl Pts',(-20.3463837743223,23.2018574804853,17.6702842363054));
#49392=CARTESIAN_POINT('Ctrl Pts',(-20.3442537144492,23.2217936658776,17.6715923831275));
#49393=CARTESIAN_POINT('Ctrl Pts',(-20.3428567994693,23.2357270598757,17.6725026542787));
#49394=CARTESIAN_POINT('Ctrl Pts',(-20.3414157510964,23.2511101373458,17.6735029225086));
#49395=CARTESIAN_POINT('Ctrl Pts',(-20.3412817510102,23.252551027927,17.6735965693101));
#49396=CARTESIAN_POINT('Ctrl Pts',(-20.3406079059697,23.2598501398061,17.6740707230023));
#49397=CARTESIAN_POINT('Ctrl Pts',(-20.3400831284815,23.2657097820843,17.674450609806));
#49398=CARTESIAN_POINT('Ctrl Pts',(-20.3389934715365,23.2782636678585,17.6752628224561));
#49399=CARTESIAN_POINT('Ctrl Pts',(-20.3384334711,23.2849583231629,17.6756949381677));
#49400=CARTESIAN_POINT('Ctrl Pts',(-20.3351183696794,23.3261392353261,17.6783465760054));
#49401=CARTESIAN_POINT('Ctrl Pts',(-20.3328976580148,23.360667966073,17.6805421273777));
#49402=CARTESIAN_POINT('Ctrl Pts',(-20.3310120703815,23.3998212624171,17.682995293457));
#49403=CARTESIAN_POINT('Ctrl Pts',(-20.330800668884,23.4044155740968,17.6832825838584));
#49404=CARTESIAN_POINT('Ctrl Pts',(-20.3304954083529,23.4113740701244,17.6837168344498));
#49405=CARTESIAN_POINT('Ctrl Pts',(-20.33039431779,23.4137379067005,17.6838641984526));
#49406=CARTESIAN_POINT('Ctrl Pts',(-20.3302229442287,23.4178513073028,17.6841203630898));
#49407=CARTESIAN_POINT('Ctrl Pts',(-20.3301514839202,23.4196008170745,17.6842292302647));
#49408=CARTESIAN_POINT('Ctrl Pts',(-20.3300047713661,23.4232659192614,17.6844571209012));
#49409=CARTESIAN_POINT('Ctrl Pts',(-20.3299298025851,23.4251815197006,17.6845761277844));
#49410=CARTESIAN_POINT('Ctrl Pts',(-20.329756440007,23.4297147875335,17.6848575177043));
#49411=CARTESIAN_POINT('Ctrl Pts',(-20.3296595281043,23.4323325177674,17.6850198167942));
#49412=CARTESIAN_POINT('Ctrl Pts',(-20.3293470039096,23.4410621248112,17.6855604295797));
#49413=CARTESIAN_POINT('Ctrl Pts',(-20.329145595566,23.4471745449709,17.6859379465033));
#49414=CARTESIAN_POINT('Ctrl Pts',(-20.3287082972051,23.4617021133822,17.6868328635982));
#49415=CARTESIAN_POINT('Ctrl Pts',(-20.3284879764787,23.4701177343231,17.6873494125506));
#49416=CARTESIAN_POINT('Ctrl Pts',(-20.3278231210125,23.4999864327357,17.689176436301));
#49417=CARTESIAN_POINT('Ctrl Pts',(-20.3275598557561,23.5214435163952,17.6904773838207));
#49418=CARTESIAN_POINT('Ctrl Pts',(-20.3273240505194,23.6248329131841,17.6966971091828));
#49419=CARTESIAN_POINT('Ctrl Pts',(-20.3302615913328,23.7067478765591,17.7014776249486));
#49420=CARTESIAN_POINT('Ctrl Pts',(-20.3481687975102,23.9483465753992,17.7153702898887));
#49421=CARTESIAN_POINT('Ctrl Pts',(-20.3719327159962,24.1071252931762,17.7242409693559));
#49422=CARTESIAN_POINT('Ctrl Pts',(-20.4584434164475,24.4883334557849,17.7461319409387));
#49423=CARTESIAN_POINT('Ctrl Pts',(-20.5334427016099,24.7070215811852,17.7592450734469));
#49424=CARTESIAN_POINT('Ctrl Pts',(-20.6373126975939,24.9290609648792,17.7741214881741));
#49425=CARTESIAN_POINT('Ctrl Pts',(-20.6435955585754,24.9422569864725,17.7750115181377));
#49426=CARTESIAN_POINT('Ctrl Pts',(-20.6523498410436,24.9603260769482,17.7762385242081));
#49427=CARTESIAN_POINT('Ctrl Pts',(-20.6547442846688,24.9652364179389,17.7765728146781));
#49428=CARTESIAN_POINT('Ctrl Pts',(-20.6585714867536,24.9730345560819,17.7771050605018));
#49429=CARTESIAN_POINT('Ctrl Pts',(-20.6599961202256,24.975926347976,17.7773027314045));
#49430=CARTESIAN_POINT('Ctrl Pts',(-20.6627720697436,24.9815398467077,17.7776870275861));
#49431=CARTESIAN_POINT('Ctrl Pts',(-20.6641229015853,24.984261790512,17.7778736357476));
#49432=CARTESIAN_POINT('Ctrl Pts',(-20.6673565524502,24.9907545620797,17.7783193973696));
#49433=CARTESIAN_POINT('Ctrl Pts',(-20.6692429194343,24.994523607525,17.7785786751864));
#49434=CARTESIAN_POINT('Ctrl Pts',(-20.6748974798819,25.0057665118734,17.7793536323631));
#49435=CARTESIAN_POINT('Ctrl Pts',(-20.6786873801292,25.0132293594935,17.779870074934));
#49436=CARTESIAN_POINT('Ctrl Pts',(-20.7040843213504,25.0627606135958,17.7833114256486));
#49437=CARTESIAN_POINT('Ctrl Pts',(-20.7265850919819,25.1043619181183,17.7862678378873));
#49438=CARTESIAN_POINT('Ctrl Pts',(-20.7806130000444,25.1992041458146,17.7931666935691));
#49439=CARTESIAN_POINT('Ctrl Pts',(-20.8127734328294,25.2520609569822,17.7971309278524));
#49440=CARTESIAN_POINT('Ctrl Pts',(-20.9082596364963,25.3992792940821,17.8085179043822));
#49441=CARTESIAN_POINT('Ctrl Pts',(-20.9750782501858,25.4912573793737,17.8160539628812));
#49442=CARTESIAN_POINT('Ctrl Pts',(-21.1427777845634,25.6981607693801,17.8339413576312));
#49443=CARTESIAN_POINT('Ctrl Pts',(-21.2472582707796,25.8098234633157,17.844351256109));
#49444=CARTESIAN_POINT('Ctrl Pts',(-21.4268043854254,25.9762715662232,17.8607831257435));
#49445=CARTESIAN_POINT('Ctrl Pts',(-21.4970063467623,26.0359683570262,17.866896329439));
#49446=CARTESIAN_POINT('Ctrl Pts',(-21.6053125587343,26.1203433784426,17.8757697598378));
#49447=CARTESIAN_POINT('Ctrl Pts',(-21.6415328908282,26.1473563632304,17.8786500559585));
#49448=CARTESIAN_POINT('Ctrl Pts',(-21.68274006518,26.1767605458619,17.8818197374122));
#49449=CARTESIAN_POINT('Ctrl Pts',(-21.6871766805196,26.1799094551112,17.8821596381275));
#49450=CARTESIAN_POINT('Ctrl Pts',(-21.693488848406,26.1843655537412,17.8826412675634));
#49451=CARTESIAN_POINT('Ctrl Pts',(-21.6953578191684,26.1856819832294,17.8827836297871));
#49452=CARTESIAN_POINT('Ctrl Pts',(-21.6987863063782,26.1880914209618,17.883044334208));
#49453=CARTESIAN_POINT('Ctrl Pts',(-21.700345393224,26.1891850371433,17.8831627185442));
#49454=CARTESIAN_POINT('Ctrl Pts',(-21.7035209145941,26.1914082987448,17.8834034951055));
#49455=CARTESIAN_POINT('Ctrl Pts',(-21.705137416757,26.1925378425761,17.8835258802623));
#49456=CARTESIAN_POINT('Ctrl Pts',(-21.7083894441172,26.1948057831869,17.8837717265871));
#49457=CARTESIAN_POINT('Ctrl Pts',(-21.7100249904788,26.1959441482594,17.8838951855432));
#49458=CARTESIAN_POINT('Ctrl Pts',(-21.7162368285864,26.2002591348075,17.8843633882847));
#49459=CARTESIAN_POINT('Ctrl Pts',(-21.7208203335501,26.2034254301845,17.8847074252938));
#49460=CARTESIAN_POINT('Ctrl Pts',(-21.7694508054668,26.2368335317796,17.8883427230564));
#49461=CARTESIAN_POINT('Ctrl Pts',(-21.8142382895746,26.2659895644503,17.891561613544));
#49462=CARTESIAN_POINT('Ctrl Pts',(-21.897355772363,26.3172007877149,17.8973432559573));
#49463=CARTESIAN_POINT('Ctrl Pts',(-21.9354527552926,26.3396059275947,17.8999225232389));
#49464=CARTESIAN_POINT('Ctrl Pts',(-22.0073597967404,26.3799278442835,17.9046830920078));
#49465=CARTESIAN_POINT('Ctrl Pts',(-22.0410439079389,26.3980356427987,17.906870386349));
#49466=CARTESIAN_POINT('Ctrl Pts',(-22.075036043603,26.4155367891046,17.9090429972639));
#49467=CARTESIAN_POINT('Origin',(-23.5502525316942,23.5502525316942,-77.3107734492734));
#49468=CARTESIAN_POINT('',(-22.0750358228142,26.4155366754296,19.4043601800006));
#49469=CARTESIAN_POINT('',(-22.0750360918396,26.4155368139396,19.1544452962233));
#49470=CARTESIAN_POINT('',(-22.0750360153461,26.4155367745563,-77.3107734492734));
#49471=CARTESIAN_POINT('Ctrl Pts',(-22.0750358228142,26.4155366754296,19.4043601800006));
#49472=CARTESIAN_POINT('Ctrl Pts',(-21.9939687733971,26.3737985929776,19.3992424347326));
#49473=CARTESIAN_POINT('Ctrl Pts',(-21.9146767412259,26.3286220321774,19.3940856294656));
#49474=CARTESIAN_POINT('Ctrl Pts',(-21.7630209617868,26.2334644961253,19.3837857518897));
#49475=CARTESIAN_POINT('Ctrl Pts',(-21.6906072610263,26.1837940049789,19.3786563162919));
#49476=CARTESIAN_POINT('Ctrl Pts',(-21.5963489247256,26.113311991075,19.3716309920995));
#49477=CARTESIAN_POINT('Ctrl Pts',(-21.5726341194396,26.0950586977324,19.3698324915126));
#49478=CARTESIAN_POINT('Ctrl Pts',(-21.5342698855086,26.0646696042408,19.3668698112217));
#49479=CARTESIAN_POINT('Ctrl Pts',(-21.5194673187915,26.0527294325543,19.3657134077547));
#49480=CARTESIAN_POINT('Ctrl Pts',(-21.5014090490665,26.0378973777065,19.364285916325));
#49481=CARTESIAN_POINT('Ctrl Pts',(-21.498052166134,26.0351288174475,19.3640198389897));
#49482=CARTESIAN_POINT('Ctrl Pts',(-21.4915500683505,26.0297441059023,19.3635030600241));
#49483=CARTESIAN_POINT('Ctrl Pts',(-21.4884042063588,26.0271287462459,19.3632523909296));
#49484=CARTESIAN_POINT('Ctrl Pts',(-21.4829425933211,26.0225705368421,19.3628160796802));
#49485=CARTESIAN_POINT('Ctrl Pts',(-21.480624574812,26.0206304015486,19.3626305487979));
#49486=CARTESIAN_POINT('Ctrl Pts',(-21.4757990232422,26.0165799521604,19.3622435830534));
#49487=CARTESIAN_POINT('Ctrl Pts',(-21.4732919738792,26.0144690694236,19.3620421249607));
#49488=CARTESIAN_POINT('Ctrl Pts',(-21.4671669892207,26.0092959741506,19.3615489217591));
#49489=CARTESIAN_POINT('Ctrl Pts',(-21.4635525890867,26.0062296037161,19.36125700556));
#49490=CARTESIAN_POINT('Ctrl Pts',(-21.4497506963997,25.9944679468523,19.3601389398655));
#49491=CARTESIAN_POINT('Ctrl Pts',(-21.4396107931277,25.9857172508981,19.3593105004364));
#49492=CARTESIAN_POINT('Ctrl Pts',(-21.2668848763215,25.8347666472278,19.3450765877454));
#49493=CARTESIAN_POINT('Ctrl Pts',(-21.118978638314,25.6766688085267,19.3309670697052));
#49494=CARTESIAN_POINT('Ctrl Pts',(-20.890236741997,25.3768393788007,19.3056351346649));
#49495=CARTESIAN_POINT('Ctrl Pts',(-20.8022160732772,25.2415237211257,19.2946381336349));
#49496=CARTESIAN_POINT('Ctrl Pts',(-20.6944896714971,25.0451368541745,19.2796395511465));
#49497=CARTESIAN_POINT('Ctrl Pts',(-20.665903620107,24.9892079957519,19.2754706720324));
#49498=CARTESIAN_POINT('Ctrl Pts',(-20.6117146366385,24.8750734769832,19.2672133221891));
#49499=CARTESIAN_POINT('Ctrl Pts',(-20.5861619348849,24.8168715701283,19.2631281095782));
#49500=CARTESIAN_POINT('Ctrl Pts',(-20.5598458390541,24.7517640199359,19.2587248604777));
#49501=CARTESIAN_POINT('Ctrl Pts',(-20.55736570862,24.7455727858205,19.2583077876028));
#49502=CARTESIAN_POINT('Ctrl Pts',(-20.5541270688489,24.7374147851807,19.2577604252961));
#49503=CARTESIAN_POINT('Ctrl Pts',(-20.5533512676259,24.7354549695498,19.2576290980631));
#49504=CARTESIAN_POINT('Ctrl Pts',(-20.5518248208036,24.7315878043744,19.2573702904512));
#49505=CARTESIAN_POINT('Ctrl Pts',(-20.5510740711862,24.729680497276,19.2572428037973));
#49506=CARTESIAN_POINT('Ctrl Pts',(-20.5496357517992,24.7260161400179,19.2569981802938));
#49507=CARTESIAN_POINT('Ctrl Pts',(-20.5489479074034,24.7242592074295,19.2568810271682));
#49508=CARTESIAN_POINT('Ctrl Pts',(-20.547369099053,24.7202160665978,19.2566117381872));
#49509=CARTESIAN_POINT('Ctrl Pts',(-20.5464792006397,24.7179294385384,19.2564596672537));
#49510=CARTESIAN_POINT('Ctrl Pts',(-20.5436607212805,24.7106627043547,19.2559771124902));
#49511=CARTESIAN_POINT('Ctrl Pts',(-20.5417418945066,24.705678786442,19.2556472167962));
#49512=CARTESIAN_POINT('Ctrl Pts',(-20.5254238854341,24.6629784996152,19.2528297288971));
#49513=CARTESIAN_POINT('Ctrl Pts',(-20.5117213950144,24.6249973011818,19.2503831860559));
#49514=CARTESIAN_POINT('Ctrl Pts',(-20.4974742566202,24.5830534531615,19.2477359113866));
#49515=CARTESIAN_POINT('Ctrl Pts',(-20.4962198009907,24.5793380578943,19.2475018809614));
#49516=CARTESIAN_POINT('Ctrl Pts',(-20.4942930392616,24.5735969012346,19.247140954578));
#49517=CARTESIAN_POINT('Ctrl Pts',(-20.4936159631903,24.5715727587486,19.2470138390893));
#49518=CARTESIAN_POINT('Ctrl Pts',(-20.4924810177359,24.5681685621686,19.2468002816303));
#49519=CARTESIAN_POINT('Ctrl Pts',(-20.4920220714973,24.5667888709415,19.2467137907331));
#49520=CARTESIAN_POINT('Ctrl Pts',(-20.4907437289591,24.562937196623,19.2464725067111));
#49521=CARTESIAN_POINT('Ctrl Pts',(-20.4899263933318,24.5604645250611,19.2463178064965));
#49522=CARTESIAN_POINT('Ctrl Pts',(-20.4875939940553,24.5533795490743,19.2458751007526));
#49523=CARTESIAN_POINT('Ctrl Pts',(-20.4860863482267,24.5487647909272,19.2455874244867));
#49524=CARTESIAN_POINT('Ctrl Pts',(-20.4810764566643,24.5333117950062,19.2446263217008));
#49525=CARTESIAN_POINT('Ctrl Pts',(-20.4776212072329,24.5224582943791,19.2439549199208));
#49526=CARTESIAN_POINT('Ctrl Pts',(-20.4423262988046,24.4095233962173,19.2370042346074));
#49527=CARTESIAN_POINT('Ctrl Pts',(-20.4155260936426,24.3059280116781,19.2309277764199));
#49528=CARTESIAN_POINT('Ctrl Pts',(-20.3520882483359,23.998322179048,19.2132659261849));
#49529=CARTESIAN_POINT('Ctrl Pts',(-20.329907442405,23.791906734035,19.2018647192872));
#49530=CARTESIAN_POINT('Ctrl Pts',(-20.3271722222006,23.5367037534076,19.1871822645609));
#49531=CARTESIAN_POINT('Ctrl Pts',(-20.3277332641241,23.4886122415337,19.1843918322158));
#49532=CARTESIAN_POINT('Ctrl Pts',(-20.332177037631,23.358139113304,19.1767362858181));
#49533=CARTESIAN_POINT('Ctrl Pts',(-20.3381457857551,23.2758697896039,19.1718161228541));
#49534=CARTESIAN_POINT('Ctrl Pts',(-20.3483027899385,23.1845695835809,19.1662210817039));
#49535=CARTESIAN_POINT('Ctrl Pts',(-20.3493845256441,23.1752189703199,19.1656464916665));
#49536=CARTESIAN_POINT('Ctrl Pts',(-20.3510404969964,23.1614339208957,19.1647970510978));
#49537=CARTESIAN_POINT('Ctrl Pts',(-20.3515830281681,23.1569956665904,19.1645232032897));
#49538=CARTESIAN_POINT('Ctrl Pts',(-20.3525528186471,23.1491969458152,19.1640413696622));
#49539=CARTESIAN_POINT('Ctrl Pts',(-20.3529761441711,23.1458359897085,19.1638335085994));
#49540=CARTESIAN_POINT('Ctrl Pts',(-20.3538094635,23.1393030164193,19.1634290630346));
#49541=CARTESIAN_POINT('Ctrl Pts',(-20.3542188819947,23.1361309285679,19.1632324969657));
#49542=CARTESIAN_POINT('Ctrl Pts',(-20.3552093077928,23.1285462734236,19.162762044955));
#49543=CARTESIAN_POINT('Ctrl Pts',(-20.3557947339459,23.1241342981496,19.1624880192802));
#49544=CARTESIAN_POINT('Ctrl Pts',(-20.35793153699,23.1082825036289,19.1615021507453));
#49545=CARTESIAN_POINT('Ctrl Pts',(-20.3595352274609,23.0968499315331,19.1607886518034));
#49546=CARTESIAN_POINT('Ctrl Pts',(-20.3871471964499,22.9074113558644,19.1489241641714));
#49547=CARTESIAN_POINT('Ctrl Pts',(-20.4279486276348,22.7319136607659,19.1372930771706));
#49548=CARTESIAN_POINT('Ctrl Pts',(-20.5454558720408,22.3676817041711,19.1118161968531));
#49549=CARTESIAN_POINT('Ctrl Pts',(-20.6258337004218,22.1809299208933,19.0979283571476));
#49550=CARTESIAN_POINT('Ctrl Pts',(-20.7649219265749,21.9268018062588,19.078545840006));
#49551=CARTESIAN_POINT('Ctrl Pts',(-20.8096804505141,21.8523344086307,19.0728070760287));
#49552=CARTESIAN_POINT('Ctrl Pts',(-20.8789163561314,21.7470290051285,19.064696294153));
#49553=CARTESIAN_POINT('Ctrl Pts',(-20.9010329188371,21.714690536262,19.0622063313632));
#49554=CARTESIAN_POINT('Ctrl Pts',(-20.9265591586669,21.678789360174,19.0594501909739));
#49555=CARTESIAN_POINT('Ctrl Pts',(-20.9293925102899,21.6748234962539,19.0591458446519));
#49556=CARTESIAN_POINT('Ctrl Pts',(-20.9336397571248,21.6689070147482,19.0586919943347));
#49557=CARTESIAN_POINT('Ctrl Pts',(-20.935046843624,21.6669515532659,19.058542022871));
#49558=CARTESIAN_POINT('Ctrl Pts',(-20.937451060458,21.6636182462294,19.0582864349631));
#49559=CARTESIAN_POINT('Ctrl Pts',(-20.9384470888343,21.6622396122766,19.0581807417731));
#49560=CARTESIAN_POINT('Ctrl Pts',(-20.9404940071553,21.6594111283792,19.0579639298355));
#49561=CARTESIAN_POINT('Ctrl Pts',(-20.9415450118077,21.6579613689445,19.0578528196451));
#49562=CARTESIAN_POINT('Ctrl Pts',(-20.9440766026882,21.654475401381,19.0575856956546));
#49563=CARTESIAN_POINT('Ctrl Pts',(-20.9455583704911,21.652440046899,19.0574297643579));
#49564=CARTESIAN_POINT('Ctrl Pts',(-20.9509677067775,21.6450280579651,19.056862039518));
#49565=CARTESIAN_POINT('Ctrl Pts',(-20.9549095856943,21.6396618139071,19.0564512357335));
#49566=CARTESIAN_POINT('Ctrl Pts',(-21.0227071630899,21.547963144304,19.049434553622));
#49567=CARTESIAN_POINT('Ctrl Pts',(-21.0908298682319,21.4648522936563,19.0431224328856));
#49568=CARTESIAN_POINT('Ctrl Pts',(-21.3042384201018,21.2295302323977,19.0248763984484));
#49569=CARTESIAN_POINT('Ctrl Pts',(-21.460403216922,21.0879628364222,19.0133648127743));
#49570=CARTESIAN_POINT('Ctrl Pts',(-21.7395193597168,20.8807540200798,18.99373476062));
#49571=CARTESIAN_POINT('Ctrl Pts',(-21.8548935695579,20.806035152707,18.9858527329255));
#49572=CARTESIAN_POINT('Ctrl Pts',(-22.0214577861786,20.712686594495,18.974515501888));
#49573=CARTESIAN_POINT('Ctrl Pts',(-22.0688871754188,20.6876400912057,18.9712927526491));
#49574=CARTESIAN_POINT('Ctrl Pts',(-22.1257271873096,20.6594149615546,18.9674287355809));
#49575=CARTESIAN_POINT('Ctrl Pts',(-22.1345569227314,20.6550806450673,18.9668284406048));
#49576=CARTESIAN_POINT('Ctrl Pts',(-22.1475081993767,20.6487965717359,18.9659478257234));
#49577=CARTESIAN_POINT('Ctrl Pts',(-22.1516143149421,20.6468150021908,18.9656686159543));
#49578=CARTESIAN_POINT('Ctrl Pts',(-22.1587911730526,20.6433702808665,18.9651805655811));
#49579=CARTESIAN_POINT('Ctrl Pts',(-22.1618600600835,20.6419032615066,18.9649718599543));
#49580=CARTESIAN_POINT('Ctrl Pts',(-22.1677965407446,20.6390769845509,18.9645681142963));
#49581=CARTESIAN_POINT('Ctrl Pts',(-22.1706638321687,20.6377170978809,18.9643730964098));
#49582=CARTESIAN_POINT('Ctrl Pts',(-22.1774715710409,20.6345006611618,18.9639100425926));
#49583=CARTESIAN_POINT('Ctrl Pts',(-22.1814137761389,20.6326478639152,18.9636418767937));
#49584=CARTESIAN_POINT('Ctrl Pts',(-22.195305189327,20.6261533893928,18.9626968369711));
#49585=CARTESIAN_POINT('Ctrl Pts',(-22.2052742624308,20.6215546051389,18.962018480617));
#49586=CARTESIAN_POINT('Ctrl Pts',(-22.33953767958,20.5604483074986,18.9528798131984));
#49587=CARTESIAN_POINT('Ctrl Pts',(-22.4672600020242,20.5118519689857,18.9441476540586));
#49588=CARTESIAN_POINT('Ctrl Pts',(-22.6859506076536,20.4441874300084,18.9291170118164));
#49589=CARTESIAN_POINT('Ctrl Pts',(-22.77536574582,20.4206827871727,18.9229526621681));
#49590=CARTESIAN_POINT('Ctrl Pts',(-23.1308653736768,20.3434023059526,18.8984721590692));
#49591=CARTESIAN_POINT('Ctrl Pts',(-23.4023012973465,20.3194780459966,18.8797455299965));
#49592=CARTESIAN_POINT('Ctrl Pts',(-23.6854704775301,20.3303183206974,18.8618832599947));
#49593=CARTESIAN_POINT('Ctrl Pts',(-23.6974030923726,20.330841570171,18.8611338474292));
#49594=CARTESIAN_POINT('Ctrl Pts',(-23.7127207889739,20.3315985995718,18.8601763094219));
#49595=CARTESIAN_POINT('Ctrl Pts',(-23.7161085867543,20.331771393231,18.8599648127063));
#49596=CARTESIAN_POINT('Ctrl Pts',(-23.7215799893495,20.3320591224571,18.8596236993352));
#49597=CARTESIAN_POINT('Ctrl Pts',(-23.7236637549415,20.332170732747,18.8594938953682));
#49598=CARTESIAN_POINT('Ctrl Pts',(-23.7276212104647,20.3323865562638,18.8592475805764));
#49599=CARTESIAN_POINT('Ctrl Pts',(-23.7294949038697,20.3324903813674,18.8591310489398));
#49600=CARTESIAN_POINT('Ctrl Pts',(-23.7337859410432,20.3327319159725,18.858864375087));
#49601=CARTESIAN_POINT('Ctrl Pts',(-23.7362032177593,20.3328707129811,18.8587142952012));
#49602=CARTESIAN_POINT('Ctrl Pts',(-23.7436470425617,20.3333065452079,18.8582525783987));
#49603=CARTESIAN_POINT('Ctrl Pts',(-23.748673083574,20.3336126385431,18.8579414513442));
#49604=CARTESIAN_POINT('Ctrl Pts',(-23.7866040565641,20.3360119321182,18.8555979691074));
#49605=CARTESIAN_POINT('Ctrl Pts',(-23.8194773706145,20.3385983056942,18.853592863262));
#49606=CARTESIAN_POINT('Ctrl Pts',(-24.0618965207586,20.3614196460397,18.8389598990507));
#49607=CARTESIAN_POINT('Ctrl Pts',(-24.2690792896872,20.4016421106844,18.8272799691827));
#49608=CARTESIAN_POINT('Ctrl Pts',(-24.6161640039729,20.5051033841715,18.807041473112));
#49609=CARTESIAN_POINT('Ctrl Pts',(-24.7582047484528,20.5586061864045,18.7985536470922));
#49610=CARTESIAN_POINT('Ctrl Pts',(-24.9912286860579,20.6656899015113,18.783723921007));
#49611=CARTESIAN_POINT('Ctrl Pts',(-25.0843098032605,20.7140969178985,18.7775388398014));
#49612=CARTESIAN_POINT('Ctrl Pts',(-25.1853490326489,20.7730732961667,18.7704536002071));
#49613=CARTESIAN_POINT('Ctrl Pts',(-25.195803515989,20.7792550532593,18.7697159437129));
#49614=CARTESIAN_POINT('Ctrl Pts',(-25.2140277012111,20.7901705546093,18.7684219601541));
#49615=CARTESIAN_POINT('Ctrl Pts',(-25.2218128112853,20.7948784075593,18.7678665798065));
#49616=CARTESIAN_POINT('Ctrl Pts',(-25.2334169036998,20.8019629742593,18.7670348091106));
#49617=CARTESIAN_POINT('Ctrl Pts',(-25.2372510607793,20.8043148490011,18.7667593327141));
#49618=CARTESIAN_POINT('Ctrl Pts',(-25.2439676326581,20.8084541761313,18.7662756181294));
#49619=CARTESIAN_POINT('Ctrl Pts',(-25.2468521793936,20.8102381702201,18.7660675077908));
#49620=CARTESIAN_POINT('Ctrl Pts',(-25.2524446884456,20.8137091640413,18.765663304303));
#49621=CARTESIAN_POINT('Ctrl Pts',(-25.2551529735356,20.8153956387586,18.7654672307376));
#49622=CARTESIAN_POINT('Ctrl Pts',(-25.2616079057645,20.819428500549,18.7649991184978));
#49623=CARTESIAN_POINT('Ctrl Pts',(-25.2653522312026,20.8217785761866,18.7647269432263));
#49624=CARTESIAN_POINT('Ctrl Pts',(-25.2787044244436,20.8301972462065,18.7637540867385));
#49625=CARTESIAN_POINT('Ctrl Pts',(-25.2882849285634,20.8363088912,18.7630518059237));
#49626=CARTESIAN_POINT('Ctrl Pts',(-25.4348154597044,20.9308785103109,18.7522448539084));
#49627=CARTESIAN_POINT('Ctrl Pts',(-25.5648695209389,21.0295381352834,18.741748724936));
#49628=CARTESIAN_POINT('Ctrl Pts',(-25.7533631149592,21.1964670687975,18.7250702899455));
#49629=CARTESIAN_POINT('Ctrl Pts',(-25.8173739142267,21.2580567549753,18.7191102224521));
#49630=CARTESIAN_POINT('Ctrl Pts',(-25.9991195617505,21.4479971116604,18.7013608192772));
#49631=CARTESIAN_POINT('Ctrl Pts',(-26.1090943648255,21.5833361132422,18.6894868539506));
#49632=CARTESIAN_POINT('Ctrl Pts',(-26.2495643839562,21.7880567003575,18.6731300066926));
#49633=CARTESIAN_POINT('Ctrl Pts',(-26.2894077053364,21.8506497652239,18.6683243633542));
#49634=CARTESIAN_POINT('Ctrl Pts',(-26.3329202173558,21.9245183921427,18.6629225602625));
#49635=CARTESIAN_POINT('Ctrl Pts',(-26.3387283964037,21.9345009100291,18.6621981112299));
#49636=CARTESIAN_POINT('Ctrl Pts',(-26.3461568706378,21.9474275950149,18.6612673503688));
#49637=CARTESIAN_POINT('Ctrl Pts',(-26.3478263029087,21.9503432076939,18.6610578977681));
#49638=CARTESIAN_POINT('Ctrl Pts',(-26.350513923626,21.9550541242638,18.6607202552193));
#49639=CARTESIAN_POINT('Ctrl Pts',(-26.3515349465715,21.9568477951727,18.6605918811234));
#49640=CARTESIAN_POINT('Ctrl Pts',(-26.353483903977,21.9602792679645,18.66034663927));
#49641=CARTESIAN_POINT('Ctrl Pts',(-26.3544121197424,21.9619168899933,18.6602297537771));
#49642=CARTESIAN_POINT('Ctrl Pts',(-26.3565325129072,21.9656654854992,18.659962544937));
#49643=CARTESIAN_POINT('Ctrl Pts',(-26.3577237422088,21.9677769893398,18.6598122836948));
#49644=CARTESIAN_POINT('Ctrl Pts',(-26.3608718725082,21.9733719251763,18.6594147914113));
#49645=CARTESIAN_POINT('Ctrl Pts',(-26.3628246879521,21.9768576694868,18.6591678241217));
#49646=CARTESIAN_POINT('Ctrl Pts',(-26.3721180914058,21.9935188356319,18.6579905570476));
#49647=CARTESIAN_POINT('Ctrl Pts',(-26.3793727676114,22.0067423279321,18.6570656962839));
#49648=CARTESIAN_POINT('Ctrl Pts',(-26.5342045727174,22.2937220276107,18.6371880973738));
#49649=CARTESIAN_POINT('Ctrl Pts',(-26.6415068501997,22.5874125034123,18.6205282053894));
#49650=CARTESIAN_POINT('Ctrl Pts',(-26.729078011321,23.007098211841,18.5962912344066));
#49651=CARTESIAN_POINT('Ctrl Pts',(-26.7467781866622,23.1234409793876,18.5895460908354));
#49652=CARTESIAN_POINT('Ctrl Pts',(-26.7648888558905,23.310987155942,18.578434092643));
#49653=CARTESIAN_POINT('Ctrl Pts',(-26.7693704969407,23.3816910617989,18.5741922271389));
#49654=CARTESIAN_POINT('Ctrl Pts',(-26.7717798780515,23.4610729241815,18.5693519043927));
#49655=CARTESIAN_POINT('Ctrl Pts',(-26.7720062722793,23.4696654452892,18.5688269623596));
#49656=CARTESIAN_POINT('Ctrl Pts',(-26.7722934633981,23.4825181333479,18.568040208278));
#49657=CARTESIAN_POINT('Ctrl Pts',(-26.7723801926752,23.4867777306864,18.5677792107976));
#49658=CARTESIAN_POINT('Ctrl Pts',(-26.7725144287698,23.4940822295859,18.5673312038727));
#49659=CARTESIAN_POINT('Ctrl Pts',(-26.7725660670323,23.4971270570738,18.5671443244059));
#49660=CARTESIAN_POINT('Ctrl Pts',(-26.7726632157123,23.5033779443067,18.5667603988557));
#49661=CARTESIAN_POINT('Ctrl Pts',(-26.7727082572685,23.5065840075025,18.5665633382302));
#49662=CARTESIAN_POINT('Ctrl Pts',(-26.7728047679902,23.5142702877264,18.5660905480944));
#49663=CARTESIAN_POINT('Ctrl Pts',(-26.7728516786828,23.5187505468328,18.5658146757019));
#49664=CARTESIAN_POINT('Ctrl Pts',(-26.7729661063602,23.532397333681,18.5649734894999));
#49665=CARTESIAN_POINT('Ctrl Pts',(-26.773003856129,23.5415640048235,18.5644072421497));
#49666=CARTESIAN_POINT('Ctrl Pts',(-26.7729774855936,23.7193191145127,18.5534029123502));
#49667=CARTESIAN_POINT('Ctrl Pts',(-26.759724207419,23.8876167449681,18.5425445142253));
#49668=CARTESIAN_POINT('Ctrl Pts',(-26.6851551362351,24.3587319883457,18.5109155132179));
#49669=CARTESIAN_POINT('Ctrl Pts',(-26.5934574051106,24.6548536111985,18.4894279314694));
#49670=CARTESIAN_POINT('Ctrl Pts',(-26.4464364805558,24.964254447275,18.4674489425529));
#49671=CARTESIAN_POINT('Ctrl Pts',(-26.4312956327195,24.994854125605,18.4652829833665));
#49672=CARTESIAN_POINT('Ctrl Pts',(-26.4133422188169,25.029732470811,18.4628280545854));
#49673=CARTESIAN_POINT('Ctrl Pts',(-26.4110030224564,25.0342505361426,18.4625103193415));
#49674=CARTESIAN_POINT('Ctrl Pts',(-26.4075420818362,25.0408966124564,18.4620433513688));
#49675=CARTESIAN_POINT('Ctrl Pts',(-26.4064286531782,25.0430289087907,18.4618935954643));
#49676=CARTESIAN_POINT('Ctrl Pts',(-26.4044408990487,25.0468252360948,18.4616270876595));
#49677=CARTESIAN_POINT('Ctrl Pts',(-26.4035675050717,25.0484897487831,18.4615102765119));
#49678=CARTESIAN_POINT('Ctrl Pts',(-26.4017275576152,25.0519888730713,18.4612648024197));
#49679=CARTESIAN_POINT('Ctrl Pts',(-26.4007606919483,25.0538233118195,18.461136160108));
#49680=CARTESIAN_POINT('Ctrl Pts',(-26.3982023953352,25.0586658430597,18.4607966978592));
#49681=CARTESIAN_POINT('Ctrl Pts',(-26.3966079636667,25.061672360482,18.4605860693574));
#49682=CARTESIAN_POINT('Ctrl Pts',(-26.3893856315562,25.0752390872169,18.4596361779436));
#49683=CARTESIAN_POINT('Ctrl Pts',(-26.3837036087039,25.0857706065013,18.4589003261876));
#49684=CARTESIAN_POINT('Ctrl Pts',(-26.2477779840406,25.3343824152357,18.4415598674329));
#49685=CARTESIAN_POINT('Ctrl Pts',(-26.0880134128168,25.5551436383689,18.4267643978409));
#49686=CARTESIAN_POINT('Ctrl Pts',(-25.7995507955885,25.8631351799909,18.4031134955261));
#49687=CARTESIAN_POINT('Ctrl Pts',(-25.6891074234568,25.9656329454133,18.3945916135063));
#49688=CARTESIAN_POINT('Ctrl Pts',(-25.5611646820118,26.0686926170247,18.3849513563897));
#49689=CARTESIAN_POINT('Ctrl Pts',(-25.5503583709244,26.0772833513782,18.3841389057398));
#49690=CARTESIAN_POINT('Ctrl Pts',(-25.5313017932551,26.0922340213092,18.3827090160906));
#49691=CARTESIAN_POINT('Ctrl Pts',(-25.523075219718,26.0986239152174,18.3820926614613));
#49692=CARTESIAN_POINT('Ctrl Pts',(-25.5077119512946,26.110438176749,18.3809431908327));
#49693=CARTESIAN_POINT('Ctrl Pts',(-25.500583308482,26.1158728807192,18.3804104575248));
#49694=CARTESIAN_POINT('Ctrl Pts',(-25.4880697714028,26.1253306059875,18.3794763311537));
#49695=CARTESIAN_POINT('Ctrl Pts',(-25.4826947708341,26.1293666692643,18.3790754204742));
#49696=CARTESIAN_POINT('Ctrl Pts',(-25.4760872761785,26.1342959554673,18.3785829643391));
#49697=CARTESIAN_POINT('Ctrl Pts',(-25.4748666970248,26.1352051799269,18.3784920106688));
#49698=CARTESIAN_POINT('Ctrl Pts',(-25.468137130815,26.1402107081172,18.3779906320603));
#49699=CARTESIAN_POINT('Ctrl Pts',(-25.4626157401535,26.1442902432589,18.3775795890068));
#49700=CARTESIAN_POINT('Ctrl Pts',(-25.4522160684438,26.1519228969457,18.3768059535564));
#49701=CARTESIAN_POINT('Ctrl Pts',(-25.4473407530092,26.155480019719,18.3764435125562));
#49702=CARTESIAN_POINT('Ctrl Pts',(-25.4220335484386,26.1738359313111,18.3745632877946));
#49703=CARTESIAN_POINT('Ctrl Pts',(-25.4014388312545,26.1884078072986,18.3730370941155));
#49704=CARTESIAN_POINT('Ctrl Pts',(-25.3729454554866,26.2080704861453,18.3709299746131));
#49705=CARTESIAN_POINT('Ctrl Pts',(-25.365192099182,26.2133710301615,18.370357047914));
#49706=CARTESIAN_POINT('Ctrl Pts',(-25.3536600198904,26.2211811284998,18.3695055075776));
#49707=CARTESIAN_POINT('Ctrl Pts',(-25.3498989417305,26.2237167518059,18.3692278817039));
#49708=CARTESIAN_POINT('Ctrl Pts',(-25.3434577233645,26.2280395060532,18.3687525783677));
#49709=CARTESIAN_POINT('Ctrl Pts',(-25.3407802260418,26.2298305796603,18.3685550500762));
#49710=CARTESIAN_POINT('Ctrl Pts',(-25.3355712931256,26.2333037276535,18.3681708574594));
#49711=CARTESIAN_POINT('Ctrl Pts',(-25.333040154162,26.2349862416059,18.3679842100195));
#49712=CARTESIAN_POINT('Ctrl Pts',(-25.3269888512035,26.2389963690301,18.3675380784522));
#49713=CARTESIAN_POINT('Ctrl Pts',(-25.323466494768,26.2413206491456,18.3672784693663));
#49714=CARTESIAN_POINT('Ctrl Pts',(-25.3129219271122,26.2482489500659,18.366501521293));
#49715=CARTESIAN_POINT('Ctrl Pts',(-25.3058863174607,26.252832424912,18.3659834131772));
#49716=CARTESIAN_POINT('Ctrl Pts',(-25.246822548433,26.2909826164312,18.3616362055157));
#49717=CARTESIAN_POINT('Ctrl Pts',(-25.1938580202495,26.3230690341703,18.3577524073316));
#49718=CARTESIAN_POINT('Ctrl Pts',(-25.0585206447413,26.3998173825195,18.3478539267582));
#49719=CARTESIAN_POINT('Ctrl Pts',(-24.9750673048491,26.4424476633357,18.3417719692439));
#49720=CARTESIAN_POINT('Ctrl Pts',(-24.6005285548807,26.6136251948325,18.3145978660624));
#49721=CARTESIAN_POINT('Ctrl Pts',(-24.2932262725778,26.7022829520062,18.292403927592));
#49722=CARTESIAN_POINT('Ctrl Pts',(-23.9384789597551,26.7497810605417,18.2693512188369));
#49723=CARTESIAN_POINT('Ctrl Pts',(-23.8989221725548,26.7543331189928,18.2668188131076));
#49724=CARTESIAN_POINT('Ctrl Pts',(-23.853994149863,26.7586613098232,18.2639933266338));
#49725=CARTESIAN_POINT('Ctrl Pts',(-23.8486979942297,26.7591582898991,18.263661054207));
#49726=CARTESIAN_POINT('Ctrl Pts',(-23.8409610393328,26.7598649891623,18.2631768398688));
#49727=CARTESIAN_POINT('Ctrl Pts',(-23.83852122824,26.7600850385761,18.2630243179845));
#49728=CARTESIAN_POINT('Ctrl Pts',(-23.8342024290891,26.7604695922494,18.2627546419912));
#49729=CARTESIAN_POINT('Ctrl Pts',(-23.8323235463584,26.7606352289548,18.2626374235443));
#49730=CARTESIAN_POINT('Ctrl Pts',(-23.828400684816,26.7609775863254,18.2623929037031));
#49731=CARTESIAN_POINT('Ctrl Pts',(-23.8263566867247,26.7611540043577,18.2622656198565));
#49732=CARTESIAN_POINT('Ctrl Pts',(-23.8210858197778,26.7616038640724,18.261937705488));
#49733=CARTESIAN_POINT('Ctrl Pts',(-23.8178586947188,26.7618743948082,18.2617372401072));
#49734=CARTESIAN_POINT('Ctrl Pts',(-23.8041533776775,26.7630025142568,18.2608871447448));
#49735=CARTESIAN_POINT('Ctrl Pts',(-23.793671275944,26.7638137046344,18.2602401102242));
#49736=CARTESIAN_POINT('Ctrl Pts',(-23.6099874905405,26.7771247452182,18.2489537321667));
#49737=CARTESIAN_POINT('Ctrl Pts',(-23.4360299109877,26.7756586374206,18.2390672455414));
#49738=CARTESIAN_POINT('Ctrl Pts',(-23.0236863167386,26.7387604178823,18.2158190635991));
#49739=CARTESIAN_POINT('Ctrl Pts',(-22.7875207352575,26.6906487727123,18.2026029839764));
#49740=CARTESIAN_POINT('Ctrl Pts',(-22.5345226184829,26.6088578677429,18.1870643707998));
#49741=CARTESIAN_POINT('Ctrl Pts',(-22.5102418371693,26.6006871832642,18.1855592673859));
#49742=CARTESIAN_POINT('Ctrl Pts',(-22.4244526234141,26.5706750705763,18.1801885299608));
#49743=CARTESIAN_POINT('Ctrl Pts',(-22.3635164086128,26.5472567355454,18.1762761226659));
#49744=CARTESIAN_POINT('Ctrl Pts',(-22.2956262906693,26.5187707591597,18.1717912697586));
#49745=CARTESIAN_POINT('Ctrl Pts',(-22.2879289994945,26.5155057703646,18.1712809348704));
#49746=CARTESIAN_POINT('Ctrl Pts',(-22.2763134255835,26.5105253250946,18.1705079859855));
#49747=CARTESIAN_POINT('Ctrl Pts',(-22.2723856680729,26.5088319435059,18.1702461258786));
#49748=CARTESIAN_POINT('Ctrl Pts',(-22.2655682641414,26.5058766346074,18.1697907579196));
#49749=CARTESIAN_POINT('Ctrl Pts',(-22.262677069916,26.504618273294,18.1695973722789));
#49750=CARTESIAN_POINT('Ctrl Pts',(-22.2566581880681,26.5019881060544,18.1691942205861));
#49751=CARTESIAN_POINT('Ctrl Pts',(-22.253530826812,26.5006155681274,18.1689844296504));
#49752=CARTESIAN_POINT('Ctrl Pts',(-22.2461594411969,26.49736642621,18.1684891889923));
#49753=CARTESIAN_POINT('Ctrl Pts',(-22.2419172850053,26.4954856256687,18.1682035954275));
#49754=CARTESIAN_POINT('Ctrl Pts',(-22.2280074702871,26.4892825937356,18.1672652081352));
#49755=CARTESIAN_POINT('Ctrl Pts',(-22.2183571290502,26.4849219066182,18.1666110920534));
#49756=CARTESIAN_POINT('Ctrl Pts',(-22.1958266452942,26.4746070637364,18.1650766336545));
#49757=CARTESIAN_POINT('Ctrl Pts',(-22.1829640647156,26.468615283051,18.1641949979318));
#49758=CARTESIAN_POINT('Ctrl Pts',(-22.1381767416871,26.4473909025699,18.1611052362202));
#49759=CARTESIAN_POINT('Ctrl Pts',(-22.1064706926468,26.4317211923938,18.1588823327108));
#49760=CARTESIAN_POINT('Ctrl Pts',(-22.0750359582753,26.4155367451729,18.1566419298442));
#49761=CARTESIAN_POINT('',(-26.77300128901,23.5530826764189,18.3151727310146));
#49762=CARTESIAN_POINT('Ctrl Pts',(-22.075036043603,26.4155367891046,17.9090429972639));
#49763=CARTESIAN_POINT('Ctrl Pts',(-22.1593709209768,26.4589573332622,17.9144332697937));
#49764=CARTESIAN_POINT('Ctrl Pts',(-22.2456017632402,26.4986436538479,17.9197342182951));
#49765=CARTESIAN_POINT('Ctrl Pts',(-22.5828848797567,26.6361659770632,17.9400867616632));
#49766=CARTESIAN_POINT('Ctrl Pts',(-22.8440119014111,26.7061771069153,17.9551681507764));
#49767=CARTESIAN_POINT('Ctrl Pts',(-23.1279342739914,26.7452586977883,17.9725320114714));
#49768=CARTESIAN_POINT('Ctrl Pts',(-23.1450985728928,26.7474806067005,17.9735848827722));
#49769=CARTESIAN_POINT('Ctrl Pts',(-23.1680935824315,26.7502691564238,17.9749998907517));
#49770=CARTESIAN_POINT('Ctrl Pts',(-23.1739093659091,26.7509583416521,17.9753581499044));
#49771=CARTESIAN_POINT('Ctrl Pts',(-23.1830070740183,26.7520113045491,17.9759191879348));
#49772=CARTESIAN_POINT('Ctrl Pts',(-23.1862877543506,26.7523858996942,17.9761216247724));
#49773=CARTESIAN_POINT('Ctrl Pts',(-23.1925680715832,26.7530932236497,17.9765093952954));
#49774=CARTESIAN_POINT('Ctrl Pts',(-23.1955676132172,26.7534267822709,17.9766947025629));
#49775=CARTESIAN_POINT('Ctrl Pts',(-23.2025871946223,26.7541974013315,17.9771286078435));
#49776=CARTESIAN_POINT('Ctrl Pts',(-23.2066075906324,26.754631109285,17.97737731143));
#49777=CARTESIAN_POINT('Ctrl Pts',(-23.2181405715713,26.755853297414,17.9780912936677));
#49778=CARTESIAN_POINT('Ctrl Pts',(-23.2256550890969,26.7566229285671,17.9785571664226));
#49779=CARTESIAN_POINT('Ctrl Pts',(-23.2738374529727,26.7613866139933,17.9815486375649));
#49780=CARTESIAN_POINT('Ctrl Pts',(-23.3145739023543,26.7646331447969,17.984097697682));
#49781=CARTESIAN_POINT('Ctrl Pts',(-23.6362581363628,26.784122380873,18.0043946255653));
#49782=CARTESIAN_POINT('Ctrl Pts',(-23.9181230683341,26.7642713426485,18.0233460331938));
#49783=CARTESIAN_POINT('Ctrl Pts',(-24.2582316810359,26.6949644254206,18.0468281372735));
#49784=CARTESIAN_POINT('Ctrl Pts',(-24.3222918716227,26.6798536289996,18.0512706168892));
#49785=CARTESIAN_POINT('Ctrl Pts',(-24.4389410612335,26.6485379508687,18.0593543410877));
#49786=CARTESIAN_POINT('Ctrl Pts',(-24.4916653341009,26.632927071347,18.0630058012206));
#49787=CARTESIAN_POINT('Ctrl Pts',(-24.556180404919,26.6120153452683,18.0674517491555));
#49788=CARTESIAN_POINT('Ctrl Pts',(-24.5683706116794,26.6079833892319,18.0682908242658));
#49789=CARTESIAN_POINT('Ctrl Pts',(-24.5844689418244,26.6025518622694,18.0693973060509));
#49790=CARTESIAN_POINT('Ctrl Pts',(-24.5883987711514,26.6012174892516,18.0696672874815));
#49791=CARTESIAN_POINT('Ctrl Pts',(-24.6434553177094,26.5824043545499,18.0734478277039));
#49792=CARTESIAN_POINT('Ctrl Pts',(-24.6941410387773,26.5636487812901,18.076905654466));
#49793=CARTESIAN_POINT('Ctrl Pts',(-24.7491707744381,26.5416969518634,18.0806165318587));
#49794=CARTESIAN_POINT('Ctrl Pts',(-24.7540022074882,26.5397560675131,18.0809419638411));
#49795=CARTESIAN_POINT('Ctrl Pts',(-24.7611639354832,26.5368588798842,18.0814237840309));
#49796=CARTESIAN_POINT('Ctrl Pts',(-24.7634978168552,26.5359115519134,18.0815807101432));
#49797=CARTESIAN_POINT('Ctrl Pts',(-24.7674893370015,26.5342859313238,18.0818489348554));
#49798=CARTESIAN_POINT('Ctrl Pts',(-24.7691475204817,26.5336089932396,18.0819603157734));
#49799=CARTESIAN_POINT('Ctrl Pts',(-24.7723792126486,26.5322865406882,18.0821772975571));
#49800=CARTESIAN_POINT('Ctrl Pts',(-24.7739527703477,26.5316411647018,18.0822829062019));
#49801=CARTESIAN_POINT('Ctrl Pts',(-24.7772125016097,26.5303012092041,18.0825015937837));
#49802=CARTESIAN_POINT('Ctrl Pts',(-24.7788985990924,26.5296064430667,18.0826146613269));
#49803=CARTESIAN_POINT('Ctrl Pts',(-24.7827541842522,26.5280138974851,18.0828731024805));
#49804=CARTESIAN_POINT('Ctrl Pts',(-24.7849232855657,26.5271151762872,18.0830184187132));
#49805=CARTESIAN_POINT('Ctrl Pts',(-24.7958446118895,26.522576165691,18.0837496888347));
#49806=CARTESIAN_POINT('Ctrl Pts',(-24.8045818495212,26.5188995944528,18.0843334526516));
#49807=CARTESIAN_POINT('Ctrl Pts',(-24.8267748971703,26.5094454360285,18.0858133331251));
#49808=CARTESIAN_POINT('Ctrl Pts',(-24.8402079436402,26.5036145224046,18.0867063433077));
#49809=CARTESIAN_POINT('Ctrl Pts',(-24.8952502273871,26.4792749973688,18.0903560648737));
#49810=CARTESIAN_POINT('Ctrl Pts',(-24.9365066850428,26.4599761078044,18.0930694824104));
#49811=CARTESIAN_POINT('Ctrl Pts',(-25.0449809601033,26.4064029766522,18.1001801172965));
#49812=CARTESIAN_POINT('Ctrl Pts',(-25.1114298614343,26.3706310768825,18.1045114866027));
#49813=CARTESIAN_POINT('Ctrl Pts',(-25.2346539171695,26.2986041549622,18.1126083357575));
#49814=CARTESIAN_POINT('Ctrl Pts',(-25.2916660278783,26.2628387740627,18.1163822846199));
#49815=CARTESIAN_POINT('Ctrl Pts',(-25.4351209230382,26.1664572524652,18.1260501961543));
#49816=CARTESIAN_POINT('Ctrl Pts',(-25.51977927485,26.1033330210452,18.1319252629363));
#49817=CARTESIAN_POINT('Ctrl Pts',(-25.7494657981449,25.9138368255922,18.1487185666196));
#49818=CARTESIAN_POINT('Ctrl Pts',(-25.8864794801201,25.7785022074225,18.1598048861253));
#49819=CARTESIAN_POINT('Ctrl Pts',(-26.0188124193252,25.6220852798301,18.1722542236531));
#49820=CARTESIAN_POINT('Ctrl Pts',(-26.026957756158,25.6123412977142,18.1730282313038));
#49821=CARTESIAN_POINT('Ctrl Pts',(-26.0379969365708,25.5989757495079,18.1740879495156));
#49822=CARTESIAN_POINT('Ctrl Pts',(-26.0409409519824,25.5953956171238,18.1743716174894));
#49823=CARTESIAN_POINT('Ctrl Pts',(-26.0459350951808,25.5892956056901,18.174854626741));
#49824=CARTESIAN_POINT('Ctrl Pts',(-26.047989161613,25.5867789476161,18.1750538081315));
#49825=CARTESIAN_POINT('Ctrl Pts',(-26.0519521045666,25.5819085049629,18.1754391050685));
#49826=CARTESIAN_POINT('Ctrl Pts',(-26.0538614734124,25.5795551245766,18.1756252003789));
#49827=CARTESIAN_POINT('Ctrl Pts',(-26.0583803260914,25.5739693565596,18.1760667146648));
#49828=CARTESIAN_POINT('Ctrl Pts',(-26.0609868802473,25.5707346155073,18.1763222513332));
#49829=CARTESIAN_POINT('Ctrl Pts',(-26.0686429142025,25.5611957638535,18.1770753744441));
#49830=CARTESIAN_POINT('Ctrl Pts',(-26.0736749293973,25.5548777342057,18.1775736611483));
#49831=CARTESIAN_POINT('Ctrl Pts',(-26.1098001095368,25.509168610678,18.181174831277));
#49832=CARTESIAN_POINT('Ctrl Pts',(-26.139991704264,25.4690767984572,18.1843133826985));
#49833=CARTESIAN_POINT('Ctrl Pts',(-26.2255943349372,25.3497018129674,18.1936079572374));
#49834=CARTESIAN_POINT('Ctrl Pts',(-26.2783832871799,25.268615414298,18.1998599632387));
#49835=CARTESIAN_POINT('Ctrl Pts',(-26.3759193915409,25.1029450781843,18.2125074272295));
#49836=CARTESIAN_POINT('Ctrl Pts',(-26.4207070191574,25.0184951409874,18.2188939977021));
#49837=CARTESIAN_POINT('Ctrl Pts',(-26.4797474821498,24.8941101254458,18.2281720852229));
#49838=CARTESIAN_POINT('Ctrl Pts',(-26.4970713378648,24.8556845488706,18.2310209836414));
#49839=CARTESIAN_POINT('Ctrl Pts',(-26.5221377235852,24.7970419296003,18.2353365054403));
#49840=CARTESIAN_POINT('Ctrl Pts',(-26.530438581115,24.7770681274158,18.2368007952246));
#49841=CARTESIAN_POINT('Ctrl Pts',(-26.5480357324656,24.7334925057867,18.239981837975));
#49842=CARTESIAN_POINT('Ctrl Pts',(-26.5572557570492,24.7098613301621,18.2416984126455));
#49843=CARTESIAN_POINT('Ctrl Pts',(-26.6197949787713,24.5438083895534,18.2536931436854));
#49844=CARTESIAN_POINT('Ctrl Pts',(-26.6632594866092,24.397861847395,18.2639001399837));
#49845=CARTESIAN_POINT('Ctrl Pts',(-26.6970703684272,24.2457157861125,18.2738744715837));
#49846=CARTESIAN_POINT('Ctrl Pts',(-26.6978777948418,24.2420522418077,18.2741142507117));
#49847=CARTESIAN_POINT('Ctrl Pts',(-26.6997733447593,24.2333795229206,18.2746809351109));
#49848=CARTESIAN_POINT('Ctrl Pts',(-26.7008559218518,24.2283691269678,18.2750075739379));
#49849=CARTESIAN_POINT('Ctrl Pts',(-26.7035826174974,24.2156019158064,18.2758379621959));
#49850=CARTESIAN_POINT('Ctrl Pts',(-26.7052100834911,24.207841523553,18.2763408869864));
#49851=CARTESIAN_POINT('Ctrl Pts',(-26.7085385716168,24.1916731712987,18.2773848129824));
#49852=CARTESIAN_POINT('Ctrl Pts',(-26.7102347026844,24.1832642454433,18.2779255584563));
#49853=CARTESIAN_POINT('Ctrl Pts',(-26.713520599817,24.1666313511673,18.2789907046412));
#49854=CARTESIAN_POINT('Ctrl Pts',(-26.7151119196564,24.1584077569837,18.2795151862882));
#49855=CARTESIAN_POINT('Ctrl Pts',(-26.7172441225985,24.1471539460552,18.2802299089252));
#49856=CARTESIAN_POINT('Ctrl Pts',(-26.7178127348494,24.1441291139079,18.2804217162835));
#49857=CARTESIAN_POINT('Ctrl Pts',(-26.7187072817134,24.1393325811412,18.2807253916173));
#49858=CARTESIAN_POINT('Ctrl Pts',(-26.7190360637595,24.1375614236127,18.2808374230448));
#49859=CARTESIAN_POINT('Ctrl Pts',(-26.7196715892146,24.1341217621749,18.2810547913491));
#49860=CARTESIAN_POINT('Ctrl Pts',(-26.7199784981517,24.1324533029505,18.2811601369571));
#49861=CARTESIAN_POINT('Ctrl Pts',(-26.7206111286237,24.1289987847561,18.2813780636562));
#49862=CARTESIAN_POINT('Ctrl Pts',(-26.7209366575876,24.1272126970475,18.2814906333223));
#49863=CARTESIAN_POINT('Ctrl Pts',(-26.7216752316503,24.1231408419372,18.2817470283648));
#49864=CARTESIAN_POINT('Ctrl Pts',(-26.7220873157904,24.1208548978728,18.2818907986511));
#49865=CARTESIAN_POINT('Ctrl Pts',(-26.7231311708739,24.1150282739246,18.2822568245388));
#49866=CARTESIAN_POINT('Ctrl Pts',(-26.7237594888756,24.1114869666606,18.2824788843357));
#49867=CARTESIAN_POINT('Ctrl Pts',(-26.7255493011093,24.1013001701885,18.2831165126908));
#49868=CARTESIAN_POINT('Ctrl Pts',(-26.726695867416,24.0946520270956,18.283531248641));
#49869=CARTESIAN_POINT('Ctrl Pts',(-26.7577276780134,23.9112840378948,18.2949332019275));
#49870=CARTESIAN_POINT('Ctrl Pts',(-26.7728438545236,23.7323568284758,18.3051144236182));
#49871=CARTESIAN_POINT('Ctrl Pts',(-26.77300128901,23.5530826764189,18.3151727310146));
#49872=CARTESIAN_POINT('Ctrl Pts',(-26.7730012867183,23.5530852849271,18.3151725846623));
#49873=CARTESIAN_POINT('Ctrl Pts',(-26.7732621727642,23.2562821006184,18.3318249468147));
#49874=CARTESIAN_POINT('Ctrl Pts',(-26.732525495111,22.9608856091882,18.3481471325133));
#49875=CARTESIAN_POINT('Ctrl Pts',(-26.6460420560006,22.6543306208819,18.3672803403713));
#49876=CARTESIAN_POINT('Ctrl Pts',(-26.6399368259007,22.6334975065806,18.3685909740539));
#49877=CARTESIAN_POINT('Ctrl Pts',(-26.6307278710816,22.6032107165283,18.3705121396507));
#49878=CARTESIAN_POINT('Ctrl Pts',(-26.6277900230134,22.5937069225832,18.3711172685335));
#49879=CARTESIAN_POINT('Ctrl Pts',(-26.6224256344382,22.576633936743,18.3722085196104));
#49880=CARTESIAN_POINT('Ctrl Pts',(-26.6200149931421,22.569059803348,18.372694117643));
#49881=CARTESIAN_POINT('Ctrl Pts',(-26.6163100688392,22.557566389597,18.3734332742031));
#49882=CARTESIAN_POINT('Ctrl Pts',(-26.6150362236821,22.553640511463,18.3736861582342));
#49883=CARTESIAN_POINT('Ctrl Pts',(-26.6127156377682,22.5465351955185,18.3741445838738));
#49884=CARTESIAN_POINT('Ctrl Pts',(-26.6116714769357,22.5433549159534,18.3743500399861));
#49885=CARTESIAN_POINT('Ctrl Pts',(-26.6095758221902,22.5370054165498,18.3747607770218));
#49886=CARTESIAN_POINT('Ctrl Pts',(-26.6085243537364,22.5338361925446,18.3749660568948));
#49887=CARTESIAN_POINT('Ctrl Pts',(-26.6055568177495,22.5249380560657,18.375543173812));
#49888=CARTESIAN_POINT('Ctrl Pts',(-26.6036295725149,22.5192129106733,18.3759153807552));
#49889=CARTESIAN_POINT('Ctrl Pts',(-26.595676057549,22.4958037894202,18.3774409195437));
#49890=CARTESIAN_POINT('Ctrl Pts',(-26.5895122598523,22.4781672351598,18.3785988086754));
#49891=CARTESIAN_POINT('Ctrl Pts',(-26.4789744263992,22.1704998815299,18.3989508001601));
#49892=CARTESIAN_POINT('Ctrl Pts',(-26.3336965646268,21.8969295658616,18.4196657769884));
#49893=CARTESIAN_POINT('Ctrl Pts',(-26.1133484598985,21.5955362451533,18.4449212373623));
#49894=CARTESIAN_POINT('Ctrl Pts',(-26.0732400943779,21.5440345327491,18.4493260544867));
#49895=CARTESIAN_POINT('Ctrl Pts',(-25.9770859141895,21.4280144950163,18.4594080168989));
#49896=CARTESIAN_POINT('Ctrl Pts',(-25.9199790797709,21.3644316439589,18.4650544604467));
#49897=CARTESIAN_POINT('Ctrl Pts',(-25.8320286235718,21.2740117349124,18.4731801369943));
#49898=CARTESIAN_POINT('Ctrl Pts',(-25.8030965238802,21.2453732219491,18.4757689307404));
#49899=CARTESIAN_POINT('Ctrl Pts',(-25.7711441438369,21.2149217665841,18.4785305447537));
#49900=CARTESIAN_POINT('Ctrl Pts',(-25.7686565191387,21.2125585645322,18.4787449208681));
#49901=CARTESIAN_POINT('Ctrl Pts',(-25.7645289691869,21.2086499825209,18.4790995764501));
#49902=CARTESIAN_POINT('Ctrl Pts',(-25.7628911965901,21.2071023490106,18.4792400289443));
#49903=CARTESIAN_POINT('Ctrl Pts',(-25.759946340738,21.2043254116858,18.479492085177));
#49904=CARTESIAN_POINT('Ctrl Pts',(-25.7586398535715,21.2030954814041,18.4796037374905));
#49905=CARTESIAN_POINT('Ctrl Pts',(-25.7561035657478,21.2007118060244,18.4798201527281));
#49906=CARTESIAN_POINT('Ctrl Pts',(-25.7548738879936,21.1995579361732,18.4799249252746));
#49907=CARTESIAN_POINT('Ctrl Pts',(-25.7523041854047,21.1971504420933,18.480143552967));
#49908=CARTESIAN_POINT('Ctrl Pts',(-25.7509639992447,21.1958970006996,18.4802573939115));
#49909=CARTESIAN_POINT('Ctrl Pts',(-25.7472501258108,21.1924294529701,18.4805723680604));
#49910=CARTESIAN_POINT('Ctrl Pts',(-25.7448741544107,21.1902177793136,18.4807733126687));
#49911=CARTESIAN_POINT('Ctrl Pts',(-25.7355151397509,21.1815322930234,18.4815626511543));
#49912=CARTESIAN_POINT('Ctrl Pts',(-25.7285066689296,21.1750857682295,18.4821489657017));
#49913=CARTESIAN_POINT('Ctrl Pts',(-25.6002702175479,21.0581764412491,18.4927924934992));
#49914=CARTESIAN_POINT('Ctrl Pts',(-25.4707933282463,20.9570777945746,18.5021745934769));
#49915=CARTESIAN_POINT('Ctrl Pts',(-25.2467827176668,20.8081892338114,18.5173125950322));
#49916=CARTESIAN_POINT('Ctrl Pts',(-25.1566178315228,20.7544133373306,18.52314633299));
#49917=CARTESIAN_POINT('Ctrl Pts',(-24.9567521127659,20.6480754642722,18.5358269566377));
#49918=CARTESIAN_POINT('Ctrl Pts',(-24.8463799447167,20.5971315203825,18.5426798235965));
#49919=CARTESIAN_POINT('Ctrl Pts',(-24.6604515300494,20.5237485305611,18.5542466855335));
#49920=CARTESIAN_POINT('Ctrl Pts',(-24.5864794401575,20.497630599832,18.5588530952495));
#49921=CARTESIAN_POINT('Ctrl Pts',(-24.4737050919773,20.4623840234399,18.5659262681683));
#49922=CARTESIAN_POINT('Ctrl Pts',(-24.4355631785849,20.451233106415,18.5683268352314));
#49923=CARTESIAN_POINT('Ctrl Pts',(-24.3899954388643,20.4388210968377,18.5712077364301));
#49924=CARTESIAN_POINT('Ctrl Pts',(-24.3827579820393,20.4368768078849,18.5716656896485));
#49925=CARTESIAN_POINT('Ctrl Pts',(-24.3716173413197,20.433925581532,18.5723712308527));
#49926=CARTESIAN_POINT('Ctrl Pts',(-24.3677189062523,20.432900684849,18.5726182353697));
#49927=CARTESIAN_POINT('Ctrl Pts',(-24.3608994532933,20.431121525746,18.573050520196));
#49928=CARTESIAN_POINT('Ctrl Pts',(-24.3579792738536,20.4303640443171,18.5732356958418));
#49929=CARTESIAN_POINT('Ctrl Pts',(-24.3518538774911,20.4287843203488,18.573624261377));
#49930=CARTESIAN_POINT('Ctrl Pts',(-24.3486484507918,20.4279629121581,18.5738276780635));
#49931=CARTESIAN_POINT('Ctrl Pts',(-24.3397325897602,20.4256928013833,18.5743937046577));
#49932=CARTESIAN_POINT('Ctrl Pts',(-24.3340194607758,20.4242548236809,18.5747566613333));
#49933=CARTESIAN_POINT('Ctrl Pts',(-24.3112653722913,20.4185939860938,18.576203279548));
#49934=CARTESIAN_POINT('Ctrl Pts',(-24.2941942211302,20.4144948030307,18.5772909298422));
#49935=CARTESIAN_POINT('Ctrl Pts',(-24.0121253996711,20.349196442041,18.5953029694333));
#49936=CARTESIAN_POINT('Ctrl Pts',(-23.7405203953988,20.3216583432215,18.6133805773614));
#49937=CARTESIAN_POINT('Ctrl Pts',(-23.3825897203145,20.3307128718005,18.637609342451));
#49938=CARTESIAN_POINT('Ctrl Pts',(-23.2965473425115,20.3363482818765,18.6434515911861));
#49939=CARTESIAN_POINT('Ctrl Pts',(-23.1170846443395,20.3553549505097,18.6555761112768));
#49940=CARTESIAN_POINT('Ctrl Pts',(-23.0238090015002,20.3693933779458,18.6618428110768));
#49941=CARTESIAN_POINT('Ctrl Pts',(-22.899165600216,20.3937871060456,18.6700628548338));
#49942=CARTESIAN_POINT('Ctrl Pts',(-22.8671506764707,20.4005604483396,18.672160164801));
#49943=CARTESIAN_POINT('Ctrl Pts',(-22.8182797019714,20.4116802458582,18.6753345097436));
#49944=CARTESIAN_POINT('Ctrl Pts',(-22.8013473819751,20.4156773888759,18.6764292834792));
#49945=CARTESIAN_POINT('Ctrl Pts',(-22.780695277739,20.4207295457401,18.6777576922173));
#49946=CARTESIAN_POINT('Ctrl Pts',(-22.7769443718859,20.4216542869404,18.6779986845668));
#49947=CARTESIAN_POINT('Ctrl Pts',(-22.7714365377854,20.4230226882679,18.6783521404281));
#49948=CARTESIAN_POINT('Ctrl Pts',(-22.7696783246011,20.4234610846603,18.6784649081997));
#49949=CARTESIAN_POINT('Ctrl Pts',(-22.7662764963319,20.4243123514623,18.6786829713214));
#49950=CARTESIAN_POINT('Ctrl Pts',(-22.7646328365011,20.4247250355764,18.6787882773996));
#49951=CARTESIAN_POINT('Ctrl Pts',(-22.7612380125919,20.4255802427166,18.6790056620811));
#49952=CARTESIAN_POINT('Ctrl Pts',(-22.7594868993271,20.4260229403287,18.6791177300608));
#49953=CARTESIAN_POINT('Ctrl Pts',(-22.7547294404244,20.4272299259531,18.6794220294055));
#49954=CARTESIAN_POINT('Ctrl Pts',(-22.7517238146208,20.4279970852396,18.6796140933608));
#49955=CARTESIAN_POINT('Ctrl Pts',(-22.7404520246233,20.4308914504133,18.6803337044668));
#49956=CARTESIAN_POINT('Ctrl Pts',(-22.7321931188203,20.4330471779246,18.6808596089252));
#49957=CARTESIAN_POINT('Ctrl Pts',(-22.5903807423052,20.4706652579848,18.6898679916159));
#49958=CARTESIAN_POINT('Ctrl Pts',(-22.4592159993945,20.5146534782014,18.6978688355037));
#49959=CARTESIAN_POINT('Ctrl Pts',(-22.2030351178869,20.6193293121198,18.7135601885615));
#49960=CARTESIAN_POINT('Ctrl Pts',(-22.0783139288904,20.6799381972539,18.7212359910517));
#49961=CARTESIAN_POINT('Ctrl Pts',(-21.8245308789571,20.8241698444795,18.7375998408844));
#49962=CARTESIAN_POINT('Ctrl Pts',(-21.6967770383129,20.9093693211074,18.7462908924542));
#49963=CARTESIAN_POINT('Ctrl Pts',(-21.5345049896295,21.0351817804683,18.758362427032));
#49964=CARTESIAN_POINT('Ctrl Pts',(-21.4942072190887,21.0680163905278,18.7614522388853));
#49965=CARTESIAN_POINT('Ctrl Pts',(-21.4402540199457,21.1141929007656,18.7657273202795));
#49966=CARTESIAN_POINT('Ctrl Pts',(-21.4258957077714,21.1267038307557,18.766878870827));
#49967=CARTESIAN_POINT('Ctrl Pts',(-21.4016282934038,21.1482302826906,18.7688493901622));
#49968=CARTESIAN_POINT('Ctrl Pts',(-21.3916628719584,21.1571817691656,18.7696656827057));
#49969=CARTESIAN_POINT('Ctrl Pts',(-21.3779779927971,21.1696293065327,18.7707966233747));
#49970=CARTESIAN_POINT('Ctrl Pts',(-21.3742105029472,21.1730725424693,18.7711090296579));
#49971=CARTESIAN_POINT('Ctrl Pts',(-21.3678694926731,21.1788955110008,18.7716366269148));
#49972=CARTESIAN_POINT('Ctrl Pts',(-21.3652916374998,21.1812705268479,18.7718516164624));
#49973=CARTESIAN_POINT('Ctrl Pts',(-21.3602023552384,21.1859747308603,18.7722770518383));
#49974=CARTESIAN_POINT('Ctrl Pts',(-21.3576907563221,21.1883037270129,18.772487489294));
#49975=CARTESIAN_POINT('Ctrl Pts',(-21.3521683077166,21.1934410715056,18.7729512600517));
#49976=CARTESIAN_POINT('Ctrl Pts',(-21.3491591203794,21.1962511916357,18.7732046693508));
#49977=CARTESIAN_POINT('Ctrl Pts',(-21.338694461284,21.206061190054,18.7740883688125));
#49978=CARTESIAN_POINT('Ctrl Pts',(-21.3312669887428,21.2130907270002,18.7747199380871));
#49979=CARTESIAN_POINT('Ctrl Pts',(-21.2567314689116,21.2843085072664,18.7811021342728));
#49980=CARTESIAN_POINT('Ctrl Pts',(-21.1924002714926,21.3513275601838,18.786976779649));
#49981=CARTESIAN_POINT('Ctrl Pts',(-21.0245305144246,21.5420586050068,18.8033763816188));
#49982=CARTESIAN_POINT('Ctrl Pts',(-20.9272497692448,21.6709016278839,18.8141281244192));
#49983=CARTESIAN_POINT('Ctrl Pts',(-20.7633689273673,21.9256084155561,18.8345781253659));
#49984=CARTESIAN_POINT('Ctrl Pts',(-20.6946504529148,22.0496770256632,18.8442204537916));
#49985=CARTESIAN_POINT('Ctrl Pts',(-20.608087421323,22.2335991202733,18.8577764202769));
#49986=CARTESIAN_POINT('Ctrl Pts',(-20.5834584653595,22.2900757257041,18.8618435316533));
#49987=CARTESIAN_POINT('Ctrl Pts',(-20.5410451240753,22.3954824301734,18.8692186858429));
#49988=CARTESIAN_POINT('Ctrl Pts',(-20.5227977498563,22.4442048250223,18.8725452832844));
#49989=CARTESIAN_POINT('Ctrl Pts',(-20.5038544929749,22.4987728638809,18.8761637403054));
#49990=CARTESIAN_POINT('Ctrl Pts',(-20.5019867559543,22.5041998256637,18.8765224406163));
#49991=CARTESIAN_POINT('Ctrl Pts',(-20.4992878364492,22.5121105134405,18.8770435777598));
#49992=CARTESIAN_POINT('Ctrl Pts',(-20.4984451817377,22.5145902698713,18.8772066913998));
#49993=CARTESIAN_POINT('Ctrl Pts',(-20.49699098988,22.5188868378188,18.8774888807997));
#49994=CARTESIAN_POINT('Ctrl Pts',(-20.4963780500238,22.5207031703242,18.8776080404735));
#49995=CARTESIAN_POINT('Ctrl Pts',(-20.495208311564,22.5241797068842,18.8778358609589));
#49996=CARTESIAN_POINT('Ctrl Pts',(-20.4946512462187,22.5258398155485,18.8779445377943));
#49997=CARTESIAN_POINT('Ctrl Pts',(-20.4933445366224,22.529744485591,18.8781998915076));
#49998=CARTESIAN_POINT('Ctrl Pts',(-20.4925960097676,22.5319894239958,18.8783465015648));
#49999=CARTESIAN_POINT('Ctrl Pts',(-20.490399470245,22.5386014195644,18.8787777213208));
#50000=CARTESIAN_POINT('Ctrl Pts',(-20.4889583279969,22.5429707789737,18.879061924823));
#50001=CARTESIAN_POINT('Ctrl Pts',(-20.4704684067996,22.5994360673582,18.8827251092045));
#50002=CARTESIAN_POINT('Ctrl Pts',(-20.4547408247555,22.6519595033828,18.8860273484791));
#50003=CARTESIAN_POINT('Ctrl Pts',(-20.4357700432927,22.7217463307329,18.890308460098));
#50004=CARTESIAN_POINT('Ctrl Pts',(-20.4313178155637,22.7386676901932,18.8913383433506));
#50005=CARTESIAN_POINT('Ctrl Pts',(-20.4136595489179,22.8080727210672,18.8955322877156));
#50006=CARTESIAN_POINT('Ctrl Pts',(-20.40163819652,22.8608508378501,18.8986510384199));
#50007=CARTESIAN_POINT('Ctrl Pts',(-20.3449352062036,23.1423682602968,18.915030973668));
#50008=CARTESIAN_POINT('Ctrl Pts',(-20.3238344023615,23.3751464847635,18.9277386686169));
#50009=CARTESIAN_POINT('Ctrl Pts',(-20.330475670023,23.744618609732,18.9488393677481));
#50010=CARTESIAN_POINT('Ctrl Pts',(-20.3415920672979,23.880755601025,18.956803959716));
#50011=CARTESIAN_POINT('Ctrl Pts',(-20.3644152311688,24.0371027580157,18.9663551127334));
#50012=CARTESIAN_POINT('Ctrl Pts',(-20.3677436420847,24.0584056392652,18.9676650689775));
#50013=CARTESIAN_POINT('Ctrl Pts',(-20.3722905562745,24.0857081101304,18.9693554722631));
#50014=CARTESIAN_POINT('Ctrl Pts',(-20.3733127918394,24.0917401882549,18.9697296653212));
#50015=CARTESIAN_POINT('Ctrl Pts',(-20.3749854454469,24.1014425053354,18.9703327146693));
#50016=CARTESIAN_POINT('Ctrl Pts',(-20.3756250686452,24.1051146106994,18.97056122673));
#50017=CARTESIAN_POINT('Ctrl Pts',(-20.3768539265151,24.1120978538251,18.9709963082669));
#50018=CARTESIAN_POINT('Ctrl Pts',(-20.3774419769011,24.1154091972396,18.9712028397155));
#50019=CARTESIAN_POINT('Ctrl Pts',(-20.3787922663608,24.1229442187455,18.9716733154238));
#50020=CARTESIAN_POINT('Ctrl Pts',(-20.3795577604538,24.1271673003994,18.9719373632407));
#50021=CARTESIAN_POINT('Ctrl Pts',(-20.3819096868659,24.1399963400945,18.9727406140464));
#50022=CARTESIAN_POINT('Ctrl Pts',(-20.3835227281266,24.1485973241805,18.9732806658422));
#50023=CARTESIAN_POINT('Ctrl Pts',(-20.3952090735637,24.2095395882958,18.9771181766755));
#50024=CARTESIAN_POINT('Ctrl Pts',(-20.4065439988443,24.2616277887642,18.9804558235301));
#50025=CARTESIAN_POINT('Ctrl Pts',(-20.4221885535364,24.3258144965168,18.9846439589303));
#50026=CARTESIAN_POINT('Ctrl Pts',(-20.4252859842404,24.3382022017755,18.9854557414291));
#50027=CARTESIAN_POINT('Ctrl Pts',(-20.4328415525951,24.3676741434262,18.9873954510713));
#50028=CARTESIAN_POINT('Ctrl Pts',(-20.4373665964263,24.3847406613282,18.9885254237405));
#50029=CARTESIAN_POINT('Ctrl Pts',(-20.4498479845517,24.4303004588519,18.9915600234238));
#50030=CARTESIAN_POINT('Ctrl Pts',(-20.4580566691105,24.4587223277285,18.9934721549165));
#50031=CARTESIAN_POINT('Ctrl Pts',(-20.4834009050462,24.5421484494063,18.9991407505608));
#50032=CARTESIAN_POINT('Ctrl Pts',(-20.5016207954039,24.5968089696668,19.0029273106996));
#50033=CARTESIAN_POINT('Ctrl Pts',(-20.5795558501787,24.8112748608555,19.0180597082608));
#50034=CARTESIAN_POINT('Ctrl Pts',(-20.6504514343432,24.9667139841629,19.0296612606917));
#50035=CARTESIAN_POINT('Ctrl Pts',(-20.8147837710453,25.2624029041648,19.0525020611909));
#50036=CARTESIAN_POINT('Ctrl Pts',(-20.9075920906761,25.4024430332882,19.0637055765542));
#50037=CARTESIAN_POINT('Ctrl Pts',(-21.0155672199061,25.5406156962828,19.0747119513928));
#50038=CARTESIAN_POINT('Ctrl Pts',(-21.02026130586,25.5465790472532,19.0751868492034));
#50039=CARTESIAN_POINT('Ctrl Pts',(-21.026754427525,25.5547682014029,19.0758387657944));
#50040=CARTESIAN_POINT('Ctrl Pts',(-21.0285353799432,25.5570082115343,19.0760170626121));
#50041=CARTESIAN_POINT('Ctrl Pts',(-21.0315455938497,25.5607840020739,19.0763175565553));
#50042=CARTESIAN_POINT('Ctrl Pts',(-21.032773277803,25.5623210291393,19.0764398671393));
#50043=CARTESIAN_POINT('Ctrl Pts',(-21.0351945148126,25.5653466671435,19.0766806087399));
#50044=CARTESIAN_POINT('Ctrl Pts',(-21.0363879825817,25.5668353422307,19.076799045586));
#50045=CARTESIAN_POINT('Ctrl Pts',(-21.0390230075859,25.5701161730401,19.0770600374898));
#50046=CARTESIAN_POINT('Ctrl Pts',(-21.0404651652092,25.5719078503611,19.0772025490961));
#50047=CARTESIAN_POINT('Ctrl Pts',(-21.0455133438864,25.5781657729807,19.0777002553674));
#50048=CARTESIAN_POINT('Ctrl Pts',(-21.0491294061749,25.5826239606709,19.0780547276707));
#50049=CARTESIAN_POINT('Ctrl Pts',(-21.0859741687391,25.6278020405361,19.081646143433));
#50050=CARTESIAN_POINT('Ctrl Pts',(-21.120184686196,25.6677158398477,19.0848132050792));
#50051=CARTESIAN_POINT('Ctrl Pts',(-21.1588808458317,25.7106892303487,19.0882393912895));
#50052=CARTESIAN_POINT('Ctrl Pts',(-21.1624126725212,25.7145921715007,19.0885507174151));
#50053=CARTESIAN_POINT('Ctrl Pts',(-21.1840586759457,25.7383951993707,19.0904504734818));
#50054=CARTESIAN_POINT('Ctrl Pts',(-21.2024124244594,25.7580769373223,19.0920258431045));
#50055=CARTESIAN_POINT('Ctrl Pts',(-21.4104717479984,25.9756614424703,19.1095239240565));
#50056=CARTESIAN_POINT('Ctrl Pts',(-21.6244484203686,26.1488240801276,19.1243133314771));
#50057=CARTESIAN_POINT('Ctrl Pts',(-21.9286096189419,26.336525848778,19.1447236161856));
#50058=CARTESIAN_POINT('Ctrl Pts',(-22.0010828502014,26.3774613466915,19.1495385378434));
#50059=CARTESIAN_POINT('Ctrl Pts',(-22.0750360918396,26.4155368139396,19.1544452962233));
#50060=CARTESIAN_POINT('Origin',(-23.5502525316942,23.5502525316942,-77.3107734492734));
#50061=CARTESIAN_POINT('',(-22.075036015346,26.4155367745563,20.6506247785903));
#50062=CARTESIAN_POINT('',(-22.0750362907684,26.4155369163599,20.4058188292237));
#50063=CARTESIAN_POINT('',(-22.0750360153461,26.4155367745563,-77.3107734492734));
#50064=CARTESIAN_POINT('',(-26.7730011713685,23.5472761317935,19.8107470580795));
#50065=CARTESIAN_POINT('Ctrl Pts',(-22.075036015346,26.4155367745563,20.6506247785903));
#50066=CARTESIAN_POINT('Ctrl Pts',(-22.072560474055,26.4142622205889,20.6504507389726));
#50067=CARTESIAN_POINT('Ctrl Pts',(-22.0700865732599,26.4129844525941,20.6502768975117));
#50068=CARTESIAN_POINT('Ctrl Pts',(-22.0654139248161,26.4105633566968,20.6499487107652));
#50069=CARTESIAN_POINT('Ctrl Pts',(-22.0632148371251,26.4094206972861,20.6497943238681));
#50070=CARTESIAN_POINT('Ctrl Pts',(-22.0594384410939,26.4074529234129,20.6495293211251));
#50071=CARTESIAN_POINT('Ctrl Pts',(-22.0578604987564,26.4066290389546,20.6494186272314));
#50072=CARTESIAN_POINT('Ctrl Pts',(-22.0546035330675,26.4049250574096,20.6491902236996));
#50073=CARTESIAN_POINT('Ctrl Pts',(-22.0529246068518,26.4040447879155,20.6490725259673));
#50074=CARTESIAN_POINT('Ctrl Pts',(-22.04898654242,26.4019756089116,20.6487965514193));
#50075=CARTESIAN_POINT('Ctrl Pts',(-22.0467280324998,26.4007854924081,20.6486383516743));
#50076=CARTESIAN_POINT('Ctrl Pts',(-22.0395072967062,26.3969695734542,20.648132795953));
#50077=CARTESIAN_POINT('Ctrl Pts',(-22.0345504821422,26.3943334691845,20.6477860929522));
#50078=CARTESIAN_POINT('Ctrl Pts',(-21.991076657609,26.371067538132,20.6447481438429));
#50079=CARTESIAN_POINT('Ctrl Pts',(-21.952973697836,26.3496680949984,20.6421049480978));
#50080=CARTESIAN_POINT('Ctrl Pts',(-21.8439751245489,26.2855017334446,20.6345659071814));
#50081=CARTESIAN_POINT('Ctrl Pts',(-21.7742738814189,26.2407678530585,20.6297724084636));
#50082=CARTESIAN_POINT('Ctrl Pts',(-21.5196112404683,26.0631125329695,20.6120673256177));
#50083=CARTESIAN_POINT('Ctrl Pts',(-21.3471863889556,25.9134021019666,20.5996385350445));
#50084=CARTESIAN_POINT('Ctrl Pts',(-21.0870901019026,25.6341505812422,20.5778787888727));
#50085=CARTESIAN_POINT('Ctrl Pts',(-20.9904176757937,25.5141862844442,20.568889559747));
#50086=CARTESIAN_POINT('Ctrl Pts',(-20.8962786959699,25.3785487079577,20.5588475412572));
#50087=CARTESIAN_POINT('Ctrl Pts',(-20.8899151182754,25.3692766850782,20.5581617309221));
#50088=CARTESIAN_POINT('Ctrl Pts',(-20.8811288676558,25.356329993468,20.5572049515081));
#50089=CARTESIAN_POINT('Ctrl Pts',(-20.8786649447082,25.3526833061227,20.5569355470693));
#50090=CARTESIAN_POINT('Ctrl Pts',(-20.8744306518186,25.3463886555988,20.5564706722689));
#50091=CARTESIAN_POINT('Ctrl Pts',(-20.8726567187406,25.3437430866623,20.5562753368408));
#50092=CARTESIAN_POINT('Ctrl Pts',(-20.8690004286177,25.3382727343037,20.5558715266286));
#50093=CARTESIAN_POINT('Ctrl Pts',(-20.8671186075487,25.33544759951,20.5556630320064));
#50094=CARTESIAN_POINT('Ctrl Pts',(-20.8627435884399,25.3288569390012,20.5551767579921));
#50095=CARTESIAN_POINT('Ctrl Pts',(-20.8602538396143,25.3250891422138,20.5548988493104));
#50096=CARTESIAN_POINT('Ctrl Pts',(-20.8524801731188,25.3132711333183,20.554027432081));
#50097=CARTESIAN_POINT('Ctrl Pts',(-20.8472244479114,25.3052025205593,20.5534328679231));
#50098=CARTESIAN_POINT('Ctrl Pts',(-20.7962497567405,25.2261737270593,20.5476128702779));
#50099=CARTESIAN_POINT('Ctrl Pts',(-20.7533030862974,25.1534726570134,20.5422851310259));
#50100=CARTESIAN_POINT('Ctrl Pts',(-20.679298253231,25.0161530779108,20.5322550777931));
#50101=CARTESIAN_POINT('Ctrl Pts',(-20.6474457364108,24.9520208499752,20.5275836421032));
#50102=CARTESIAN_POINT('Ctrl Pts',(-20.5343016784098,24.7037891627103,20.5095675508202));
#50103=CARTESIAN_POINT('Ctrl Pts',(-20.4681824127434,24.5132886660916,20.4958398508168));
#50104=CARTESIAN_POINT('Ctrl Pts',(-20.3849977282559,24.1741083888681,20.4723216071046));
#50105=CARTESIAN_POINT('Ctrl Pts',(-20.3596792667438,24.0280475681586,20.4624879847602));
#50106=CARTESIAN_POINT('Ctrl Pts',(-20.3435301800228,23.8714028824876,20.4525844135398));
#50107=CARTESIAN_POINT('Ctrl Pts',(-20.3426077769034,23.8620552270192,20.4519958637404));
#50108=CARTESIAN_POINT('Ctrl Pts',(-20.3414234118372,23.8494909888088,20.4512081868314));
#50109=CARTESIAN_POINT('Ctrl Pts',(-20.341125405344,23.8462779728308,20.4510070547097));
#50110=CARTESIAN_POINT('Ctrl Pts',(-20.3406658571961,23.8412410094248,20.4506922181251));
#50111=CARTESIAN_POINT('Ctrl Pts',(-20.3405010445339,23.8394173739571,20.4505783285407));
#50112=CARTESIAN_POINT('Ctrl Pts',(-20.3401873637631,23.8359132157796,20.450359675045));
#50113=CARTESIAN_POINT('Ctrl Pts',(-20.3400382620349,23.8342327276363,20.4502548986893));
#50114=CARTESIAN_POINT('Ctrl Pts',(-20.3396881061396,23.8302506912446,20.4500068200053));
#50115=CARTESIAN_POINT('Ctrl Pts',(-20.3394882074012,23.8279490457455,20.4498635839705));
#50116=CARTESIAN_POINT('Ctrl Pts',(-20.3389149508691,23.8212651656581,20.4494480781631));
#50117=CARTESIAN_POINT('Ctrl Pts',(-20.3385480866145,23.8168823570847,20.4491761752683));
#50118=CARTESIAN_POINT('Ctrl Pts',(-20.3359474792782,23.7850294214405,20.4472040170497));
#50119=CARTESIAN_POINT('Ctrl Pts',(-20.3340571413745,23.7575313103799,20.4455228291897));
#50120=CARTESIAN_POINT('Ctrl Pts',(-20.3291479997729,23.6696562541669,20.4402087644271));
#50121=CARTESIAN_POINT('Ctrl Pts',(-20.3274748216364,23.6092141864215,20.4366415889358));
#50122=CARTESIAN_POINT('Ctrl Pts',(-20.3276020837555,23.3349905464978,20.4207134310528));
#50123=CARTESIAN_POINT('Ctrl Pts',(-20.3489695094329,23.1217494828009,20.4090022161768));
#50124=CARTESIAN_POINT('Ctrl Pts',(-20.432139291801,22.7099932727689,20.3853798340065));
#50125=CARTESIAN_POINT('Ctrl Pts',(-20.4922881997836,22.5122252915948,20.3735373528332));
#50126=CARTESIAN_POINT('Ctrl Pts',(-20.5757325587474,22.3098863033267,20.3602378319656));
#50127=CARTESIAN_POINT('Ctrl Pts',(-20.5806220487365,22.2982252806014,20.3594671848225));
#50128=CARTESIAN_POINT('Ctrl Pts',(-20.5873940502132,22.2823374771766,20.3584113757057));
#50129=CARTESIAN_POINT('Ctrl Pts',(-20.5892172723998,22.2780854201839,20.3581282369605));
#50130=CARTESIAN_POINT('Ctrl Pts',(-20.5923352640829,22.2708567614023,20.357645909961));
#50131=CARTESIAN_POINT('Ctrl Pts',(-20.5936253902236,22.2678781537225,20.3574468806562));
#50132=CARTESIAN_POINT('Ctrl Pts',(-20.5961289047747,22.2621219689643,20.357061703376));
#50133=CARTESIAN_POINT('Ctrl Pts',(-20.5973417161966,22.2593441440145,20.3568755753546));
#50134=CARTESIAN_POINT('Ctrl Pts',(-20.6002281053644,22.2527585059289,20.3564337123175));
#50135=CARTESIAN_POINT('Ctrl Pts',(-20.6019051364866,22.2489522205618,20.3561778590329));
#50136=CARTESIAN_POINT('Ctrl Pts',(-20.6067840440001,22.2379366204899,20.3554360344297));
#50137=CARTESIAN_POINT('Ctrl Pts',(-20.6100050104238,22.2307358395915,20.3549494074501));
#50138=CARTESIAN_POINT('Ctrl Pts',(-20.6338937235263,22.1778520961784,20.3513628785029));
#50139=CARTESIAN_POINT('Ctrl Pts',(-20.6555976704853,22.1326473574772,20.3482273276369));
#50140=CARTESIAN_POINT('Ctrl Pts',(-20.7298966080705,21.9867251649323,20.3378673877354));
#50141=CARTESIAN_POINT('Ctrl Pts',(-20.7867589832719,21.8882886703817,20.3304961124719));
#50142=CARTESIAN_POINT('Ctrl Pts',(-20.9362060749194,21.658523339557,20.3123662560774));
#50143=CARTESIAN_POINT('Ctrl Pts',(-21.0336421296137,21.5307120466303,20.301482905443));
#50144=CARTESIAN_POINT('Ctrl Pts',(-21.2039269233998,21.3388971849937,20.2841336404195));
#50145=CARTESIAN_POINT('Ctrl Pts',(-21.2708498916183,21.2699758835756,20.2776616171758));
#50146=CARTESIAN_POINT('Ctrl Pts',(-21.4074702823327,21.14131067269,20.2652401078896));
#50147=CARTESIAN_POINT('Ctrl Pts',(-21.4768450024346,21.0813455736983,20.2592859857762));
#50148=CARTESIAN_POINT('Ctrl Pts',(-21.55373587608,21.0204145385827,20.2531355324438));
#50149=CARTESIAN_POINT('Ctrl Pts',(-21.5587947480632,21.0164303348454,20.2527328785433));
#50150=CARTESIAN_POINT('Ctrl Pts',(-21.5658200780055,21.0109314492602,20.2521765149781));
#50151=CARTESIAN_POINT('Ctrl Pts',(-21.5677763513883,21.0094038707999,20.2520218903603));
#50152=CARTESIAN_POINT('Ctrl Pts',(-21.5711394668655,21.0067839921988,20.2517565867457));
#50153=CARTESIAN_POINT('Ctrl Pts',(-21.5725454493427,21.0056905986239,20.2516458293041));
#50154=CARTESIAN_POINT('Ctrl Pts',(-21.5754492925373,21.0034362209715,20.2514173981795));
#50155=CARTESIAN_POINT('Ctrl Pts',(-21.5769472679677,21.0022753948047,20.2512997362533));
#50156=CARTESIAN_POINT('Ctrl Pts',(-21.5804627221012,20.9995561233638,20.2510240184491));
#50157=CARTESIAN_POINT('Ctrl Pts',(-21.5824810328613,20.9979987453448,20.2508660392221));
#50158=CARTESIAN_POINT('Ctrl Pts',(-21.5889348320804,20.9930310419869,20.2503618862016));
#50159=CARTESIAN_POINT('Ctrl Pts',(-21.5933773854662,20.9896298477696,20.2500163602798));
#50160=CARTESIAN_POINT('Ctrl Pts',(-21.6502078962411,20.946355002237,20.2456152566793));
#50161=CARTESIAN_POINT('Ctrl Pts',(-21.7038014176244,20.9080807497137,20.2416701138543));
#50162=CARTESIAN_POINT('Ctrl Pts',(-21.8097386442837,20.8372240045645,20.2341811529989));
#50163=CARTESIAN_POINT('Ctrl Pts',(-21.8619170329008,20.8044491155372,20.2306294269077));
#50164=CARTESIAN_POINT('Ctrl Pts',(-22.0430566289472,20.6977868229801,20.21864751512));
#50165=CARTESIAN_POINT('Ctrl Pts',(-22.1761739706156,20.6313295401935,20.2104183943869));
#50166=CARTESIAN_POINT('Ctrl Pts',(-22.4291889204723,20.5261733060566,20.195068347843));
#50167=CARTESIAN_POINT('Ctrl Pts',(-22.5476748270093,20.4848531222669,20.1879894423084));
#50168=CARTESIAN_POINT('Ctrl Pts',(-22.7719066833979,20.4210501230689,20.1744694255498));
#50169=CARTESIAN_POINT('Ctrl Pts',(-22.8769572253449,20.3967783284897,20.1680880655503));
#50170=CARTESIAN_POINT('Ctrl Pts',(-22.9932549748866,20.3759842024976,20.1608981705086));
#50171=CARTESIAN_POINT('Ctrl Pts',(-23.0035004444638,20.3742034364886,20.1602637405125));
#50172=CARTESIAN_POINT('Ctrl Pts',(-23.0179505484794,20.3717638543657,20.1593674504804));
#50173=CARTESIAN_POINT('Ctrl Pts',(-23.0221482201102,20.3710637186408,20.1591069057435));
#50174=CARTESIAN_POINT('Ctrl Pts',(-23.0294530816759,20.3698601968729,20.1586531877796));
#50175=CARTESIAN_POINT('Ctrl Pts',(-23.0325596526911,20.3693530435851,20.1584601345776));
#50176=CARTESIAN_POINT('Ctrl Pts',(-23.0390425591581,20.3683044461174,20.1580570564227));
#50177=CARTESIAN_POINT('Ctrl Pts',(-23.0424190213462,20.3677638230021,20.1578470056645));
#50178=CARTESIAN_POINT('Ctrl Pts',(-23.0504029657552,20.3664985009849,20.1573500415326));
#50179=CARTESIAN_POINT('Ctrl Pts',(-23.0550111640947,20.3657784300442,20.1570629815103));
#50180=CARTESIAN_POINT('Ctrl Pts',(-23.0647056121414,20.3642851402639,20.1564586117059));
#50181=CARTESIAN_POINT('Ctrl Pts',(-23.0697921785769,20.3635140926417,20.1561412337253));
#50182=CARTESIAN_POINT('Ctrl Pts',(-23.1088709830409,20.3576860190373,20.1537007807977));
#50183=CARTESIAN_POINT('Ctrl Pts',(-23.1429392146725,20.3531609903922,20.1515608971636));
#50184=CARTESIAN_POINT('Ctrl Pts',(-23.2724144644833,20.3380667884513,20.1433782420711));
#50185=CARTESIAN_POINT('Ctrl Pts',(-23.368196675357,20.3312179213867,20.1372201197725));
#50186=CARTESIAN_POINT('Ctrl Pts',(-23.626104304556,20.3243236550995,20.1203551604916));
#50187=CARTESIAN_POINT('Ctrl Pts',(-23.788155554582,20.3322153323776,20.1094472614723));
#50188=CARTESIAN_POINT('Ctrl Pts',(-24.1276121200365,20.3745315075581,20.0862940275642));
#50189=CARTESIAN_POINT('Ctrl Pts',(-24.3041469902702,20.4117493928719,20.074074409829));
#50190=CARTESIAN_POINT('Ctrl Pts',(-24.4779880759,20.4639236045081,20.0623634130065));
#50191=CARTESIAN_POINT('Ctrl Pts',(-24.4793164521329,20.4643232197168,20.0622739460019));
#50192=CARTESIAN_POINT('Ctrl Pts',(-24.4854452191336,20.4661712517186,20.0618612655817));
#50193=CARTESIAN_POINT('Ctrl Pts',(-24.4902425124173,20.4676300214071,20.0615385118575));
#50194=CARTESIAN_POINT('Ctrl Pts',(-24.5299162114739,20.4797952975062,20.0588716940903));
#50195=CARTESIAN_POINT('Ctrl Pts',(-24.5646137611495,20.4910826884122,20.0565544633859));
#50196=CARTESIAN_POINT('Ctrl Pts',(-24.6035307601066,20.5044776950365,20.0539784356544));
#50197=CARTESIAN_POINT('Ctrl Pts',(-24.6079443153364,20.5060075557545,20.0536866260606));
#50198=CARTESIAN_POINT('Ctrl Pts',(-24.6146058010105,20.508332847317,20.0532467159547));
#50199=CARTESIAN_POINT('Ctrl Pts',(-24.6168561764672,20.509121177551,20.0530981966922));
#50200=CARTESIAN_POINT('Ctrl Pts',(-24.620761898699,20.5104942617451,20.052840588665));
#50201=CARTESIAN_POINT('Ctrl Pts',(-24.6224176422898,20.5110778706678,20.0527314314958));
#50202=CARTESIAN_POINT('Ctrl Pts',(-24.6258764593825,20.5123001970292,20.0525035099681));
#50203=CARTESIAN_POINT('Ctrl Pts',(-24.6276794397758,20.512939166354,20.0523847613738));
#50204=CARTESIAN_POINT('Ctrl Pts',(-24.631979812862,20.5144675130185,20.0521016700542));
#50205=CARTESIAN_POINT('Ctrl Pts',(-24.6344766865021,20.5153583699992,20.0519374160915));
#50206=CARTESIAN_POINT('Ctrl Pts',(-24.639748929766,20.5172467851115,20.0515908227374));
#50207=CARTESIAN_POINT('Ctrl Pts',(-24.6425240374505,20.518245074894,20.051408527018));
#50208=CARTESIAN_POINT('Ctrl Pts',(-24.6652330762305,20.5264494236802,20.0499178777842));
#50209=CARTESIAN_POINT('Ctrl Pts',(-24.685097461857,20.53384839891,20.0486208891082));
#50210=CARTESIAN_POINT('Ctrl Pts',(-24.744841011723,20.5567750826569,20.0447369715125));
#50211=CARTESIAN_POINT('Ctrl Pts',(-24.7844867929744,20.5729021909588,20.0421824525041));
#50212=CARTESIAN_POINT('Ctrl Pts',(-24.9200623421056,20.6312253673563,20.0334875650309));
#50213=CARTESIAN_POINT('Ctrl Pts',(-25.0142537181823,20.677309375235,20.027517050072));
#50214=CARTESIAN_POINT('Ctrl Pts',(-25.1835357264081,20.7706240730417,20.0166305341263));
#50215=CARTESIAN_POINT('Ctrl Pts',(-25.2592416907778,20.8165179367233,20.0116998545898));
#50216=CARTESIAN_POINT('Ctrl Pts',(-25.5385387417953,21.0019727839191,19.9929551592416));
#50217=CARTESIAN_POINT('Ctrl Pts',(-25.7277219196129,21.1616098796913,19.9790121290229));
#50218=CARTESIAN_POINT('Ctrl Pts',(-25.9077998213481,21.3529031264863,19.96308235942));
#50219=CARTESIAN_POINT('Ctrl Pts',(-25.9186812437433,21.3646361305302,19.9621084122673));
#50220=CARTESIAN_POINT('Ctrl Pts',(-25.9333001271394,21.3806364631637,19.9607842104077));
#50221=CARTESIAN_POINT('Ctrl Pts',(-25.9371144927983,21.3848334717968,19.9604372283508));
#50222=CARTESIAN_POINT('Ctrl Pts',(-25.9431071649807,21.3914623785057,19.9598897581432));
#50223=CARTESIAN_POINT('Ctrl Pts',(-25.9452929011663,21.3938875695376,19.9596895844265));
#50224=CARTESIAN_POINT('Ctrl Pts',(-25.9494972664826,21.3985668156243,19.9593035886894));
#50225=CARTESIAN_POINT('Ctrl Pts',(-25.9515164147517,21.4008204015783,19.9591177888285));
#50226=CARTESIAN_POINT('Ctrl Pts',(-25.9562755687793,21.4061472031627,19.9586788490698));
#50227=CARTESIAN_POINT('Ctrl Pts',(-25.9590128600108,21.409222827253,19.9584255955199));
#50228=CARTESIAN_POINT('Ctrl Pts',(-25.9646550022389,21.4155868612522,19.9579019430556));
#50229=CARTESIAN_POINT('Ctrl Pts',(-25.9675590451417,21.4188759732056,19.9576315110176));
#50230=CARTESIAN_POINT('Ctrl Pts',(-25.9750548592444,21.4274007395656,19.9569311278913));
#50231=CARTESIAN_POINT('Ctrl Pts',(-25.9796363753429,21.4326453447889,19.9565007499159));
#50232=CARTESIAN_POINT('Ctrl Pts',(-26.0206281134546,21.4798779884141,19.9526292868828));
#50233=CARTESIAN_POINT('Ctrl Pts',(-26.0559615865926,21.522784215348,19.9491440072573));
#50234=CARTESIAN_POINT('Ctrl Pts',(-26.1694590638123,21.6681075369293,19.9374319839413));
#50235=CARTESIAN_POINT('Ctrl Pts',(-26.2425837190717,21.7742856022025,19.9290157745398));
#50236=CARTESIAN_POINT('Ctrl Pts',(-26.3324280119512,21.9230939498599,19.917437614496));
#50237=CARTESIAN_POINT('Ctrl Pts',(-26.3548921693095,21.9621272932523,19.9144203184837));
#50238=CARTESIAN_POINT('Ctrl Pts',(-26.3984164449929,22.0415596401807,19.9083266125955));
#50239=CARTESIAN_POINT('Ctrl Pts',(-26.419452868962,22.081960586013,19.9052505801569));
#50240=CARTESIAN_POINT('Ctrl Pts',(-26.527007284457,22.2996654614514,19.8888249318512));
#50241=CARTESIAN_POINT('Ctrl Pts',(-26.5979703996108,22.4842013426492,19.8753952508325));
#50242=CARTESIAN_POINT('Ctrl Pts',(-26.6517887457057,22.6747006539352,19.8626580601752));
#50243=CARTESIAN_POINT('Ctrl Pts',(-26.6519636946625,22.6753206263487,19.86261661942));
#50244=CARTESIAN_POINT('Ctrl Pts',(-26.6623614284191,22.7122097327893,19.8601515555321));
#50245=CARTESIAN_POINT('Ctrl Pts',(-26.671948059372,22.7486573350335,19.8577568637881));
#50246=CARTESIAN_POINT('Ctrl Pts',(-26.6821367671859,22.7903537737573,19.8550701721256));
#50247=CARTESIAN_POINT('Ctrl Pts',(-26.6833674441765,22.7954439911105,19.8547430788028));
#50248=CARTESIAN_POINT('Ctrl Pts',(-26.6851519636326,22.8029045278345,19.8542650003894));
#50249=CARTESIAN_POINT('Ctrl Pts',(-26.6857155288178,22.8052724775964,19.8541134558773));
#50250=CARTESIAN_POINT('Ctrl Pts',(-26.6867104956009,22.8094741897516,19.8538449042907));
#50251=CARTESIAN_POINT('Ctrl Pts',(-26.6871429722808,22.811307692701,19.8537278346775));
#50252=CARTESIAN_POINT('Ctrl Pts',(-26.6880447984773,22.8151460817064,19.8534830012882));
#50253=CARTESIAN_POINT('Ctrl Pts',(-26.6885138332297,22.8171510341922,19.8533552561223));
#50254=CARTESIAN_POINT('Ctrl Pts',(-26.6894621680707,22.8212224080561,19.8530961342577));
#50255=CARTESIAN_POINT('Ctrl Pts',(-26.6899413501817,22.8232888562484,19.8529647644553));
#50256=CARTESIAN_POINT('Ctrl Pts',(-26.6911192061183,22.8283911872046,19.8526407593817));
#50257=CARTESIAN_POINT('Ctrl Pts',(-26.6918155208285,22.831427620697,19.8524482597279));
#50258=CARTESIAN_POINT('Ctrl Pts',(-26.6937335586961,22.8398476675008,19.851915326501));
#50259=CARTESIAN_POINT('Ctrl Pts',(-26.6949458604707,22.8452334488394,19.8515754267017));
#50260=CARTESIAN_POINT('Ctrl Pts',(-26.6987739321953,22.8624463993464,19.8504921728693));
#50261=CARTESIAN_POINT('Ctrl Pts',(-26.7013369010583,22.874285378037,19.8497517341361));
#50262=CARTESIAN_POINT('Ctrl Pts',(-26.7496109339278,23.1035172561767,19.8354992558051));
#50263=CARTESIAN_POINT('Ctrl Pts',(-26.7727959465012,23.3250751626967,19.8231626665619));
#50264=CARTESIAN_POINT('Ctrl Pts',(-26.773001157321,23.547276205028,19.8107470336484));
#50265=CARTESIAN_POINT('Ctrl Pts',(-26.7730011572524,23.5472761306737,19.810747037803));
#50266=CARTESIAN_POINT('Ctrl Pts',(-26.7732080179902,23.771258098769,19.7982318944655));
#50267=CARTESIAN_POINT('Ctrl Pts',(-26.7500658446963,23.9946323456618,19.7856820690413));
#50268=CARTESIAN_POINT('Ctrl Pts',(-26.6939559325066,24.2613106454192,19.7694639610157));
#50269=CARTESIAN_POINT('Ctrl Pts',(-26.6828877456993,24.3085868526511,19.7665428526371));
#50270=CARTESIAN_POINT('Ctrl Pts',(-26.6690358335551,24.3622597248724,19.763167900945));
#50271=CARTESIAN_POINT('Ctrl Pts',(-26.667293975931,24.3689207181373,19.762748022063));
#50272=CARTESIAN_POINT('Ctrl Pts',(-26.6644156540831,24.3797852741851,19.7620614587238));
#50273=CARTESIAN_POINT('Ctrl Pts',(-26.6632919853483,24.3839922293285,19.7617951892557));
#50274=CARTESIAN_POINT('Ctrl Pts',(-26.6610954963404,24.3921494179704,19.7612780790345));
#50275=CARTESIAN_POINT('Ctrl Pts',(-26.6600236690352,24.3960999120911,19.7610272709476));
#50276=CARTESIAN_POINT('Ctrl Pts',(-26.658147181009,24.402964411624,19.7605908052699));
#50277=CARTESIAN_POINT('Ctrl Pts',(-26.6573459392905,24.4058793532612,19.7604052592023));
#50278=CARTESIAN_POINT('Ctrl Pts',(-26.6556678045662,24.4119510168808,19.7600183472402));
#50279=CARTESIAN_POINT('Ctrl Pts',(-26.6547901972954,24.4151075363621,19.7598169582459));
#50280=CARTESIAN_POINT('Ctrl Pts',(-26.6523648353984,24.4237796549975,19.7592629995069));
#50281=CARTESIAN_POINT('Ctrl Pts',(-26.6508071907041,24.4292924544245,19.7589101074531));
#50282=CARTESIAN_POINT('Ctrl Pts',(-26.6447338587181,24.4505701438646,19.7575451539757));
#50283=CARTESIAN_POINT('Ctrl Pts',(-26.6401126269463,24.4663044198852,19.7565296489241));
#50284=CARTESIAN_POINT('Ctrl Pts',(-26.5605903646619,24.7296107269387,19.7394301746216));
#50285=CARTESIAN_POINT('Ctrl Pts',(-26.456289534761,24.9672608676275,19.7223118255461));
#50286=CARTESIAN_POINT('Ctrl Pts',(-26.3020524794845,25.2282589246837,19.7018156883449));
#50287=CARTESIAN_POINT('Ctrl Pts',(-26.2785571134124,25.2661961487095,19.6987938624216));
#50288=CARTESIAN_POINT('Ctrl Pts',(-26.2311012533038,25.3393816444652,19.692891138698));
#50289=CARTESIAN_POINT('Ctrl Pts',(-26.2072139045869,25.3746672832872,19.6900105876434));
#50290=CARTESIAN_POINT('Ctrl Pts',(-26.1187212381181,25.4999600648115,19.6796771175798));
#50291=CARTESIAN_POINT('Ctrl Pts',(-26.0501793682702,25.5871032821835,19.6722875917451));
#50292=CARTESIAN_POINT('Ctrl Pts',(-25.9473997362857,25.7047514145999,19.6621936868112));
#50293=CARTESIAN_POINT('Ctrl Pts',(-25.9167983800514,25.738320500189,19.6592992743473));
#50294=CARTESIAN_POINT('Ctrl Pts',(-25.8830669111001,25.7737873424771,19.6562363191723));
#50295=CARTESIAN_POINT('Ctrl Pts',(-25.8806338806549,25.7763371554726,19.6560160868005));
#50296=CARTESIAN_POINT('Ctrl Pts',(-25.8766114007856,25.7805388876922,19.6556531369521));
#50297=CARTESIAN_POINT('Ctrl Pts',(-25.8750243706366,25.7821931031453,19.6555102344151));
#50298=CARTESIAN_POINT('Ctrl Pts',(-25.8719249074114,25.7854168865646,19.6552317253192));
#50299=CARTESIAN_POINT('Ctrl Pts',(-25.8704126448489,25.7869866157653,19.6550961056412));
#50300=CARTESIAN_POINT('Ctrl Pts',(-25.8677340267511,25.7897613829913,19.65485636295));
#50301=CARTESIAN_POINT('Ctrl Pts',(-25.8665683293519,25.7909670383901,19.6547521894062));
#50302=CARTESIAN_POINT('Ctrl Pts',(-25.8640727789466,25.7935441032749,19.6545295123336));
#50303=CARTESIAN_POINT('Ctrl Pts',(-25.8627426513436,25.7949152364879,19.6544110313541));
#50304=CARTESIAN_POINT('Ctrl Pts',(-25.85888840702,25.7988812387329,19.6540683073747));
#50305=CARTESIAN_POINT('Ctrl Pts',(-25.8563611259656,25.8014730492565,19.6538443127368));
#50306=CARTESIAN_POINT('Ctrl Pts',(-25.8450519415401,25.8130319644344,19.6528452156392));
#50307=CARTESIAN_POINT('Ctrl Pts',(-25.8362219107491,25.8219521383498,19.652073849914));
#50308=CARTESIAN_POINT('Ctrl Pts',(-25.6811006934994,25.9768365929316,19.6386692228917));
#50309=CARTESIAN_POINT('Ctrl Pts',(-25.5211299577579,26.1084735177093,19.6270868547006));
#50310=CARTESIAN_POINT('Ctrl Pts',(-25.2935589334931,26.261630055973,19.6117507860844));
#50311=CARTESIAN_POINT('Ctrl Pts',(-25.2363164516622,26.2975919131558,19.6079808065677));
#50312=CARTESIAN_POINT('Ctrl Pts',(-25.1200028285245,26.3656592524351,19.6004232380903));
#50313=CARTESIAN_POINT('Ctrl Pts',(-25.0609742534985,26.3977690716029,19.5966377712355));
#50314=CARTESIAN_POINT('Ctrl Pts',(-24.9003224223795,26.4787568289068,19.5863903346175));
#50315=CARTESIAN_POINT('Ctrl Pts',(-24.7970735399735,26.5241825595476,19.5798587432113));
#50316=CARTESIAN_POINT('Ctrl Pts',(-24.660920080862,26.5757468561927,19.5711871728024));
#50317=CARTESIAN_POINT('Ctrl Pts',(-24.630000798755,26.5869187749611,19.5692144758437));
#50318=CARTESIAN_POINT('Ctrl Pts',(-24.5795741789903,26.6042716791821,19.5659889188362));
#50319=CARTESIAN_POINT('Ctrl Pts',(-24.5601689319877,26.6107434794377,19.5647457006038));
#50320=CARTESIAN_POINT('Ctrl Pts',(-24.5364710982792,26.6183969685199,19.5632247026338));
#50321=CARTESIAN_POINT('Ctrl Pts',(-24.5322356576063,26.6197551764907,19.5629527522995));
#50322=CARTESIAN_POINT('Ctrl Pts',(-24.5240327402928,26.622366946906,19.5624258442157));
#50323=CARTESIAN_POINT('Ctrl Pts',(-24.5200656190738,26.6236216032669,19.5621709230302));
#50324=CARTESIAN_POINT('Ctrl Pts',(-24.5132041884625,26.6257770166596,19.5617298476214));
#50325=CARTESIAN_POINT('Ctrl Pts',(-24.5103110105933,26.6266813814951,19.5615438123409));
#50326=CARTESIAN_POINT('Ctrl Pts',(-24.5043176195188,26.6285455494661,19.5611583191323));
#50327=CARTESIAN_POINT('Ctrl Pts',(-24.5012172248136,26.6295047538073,19.5609588417614));
#50328=CARTESIAN_POINT('Ctrl Pts',(-24.4927882405287,26.6320985800857,19.5604163582315));
#50329=CARTESIAN_POINT('Ctrl Pts',(-24.4874568689306,26.6337240587324,19.5600730524032));
#50330=CARTESIAN_POINT('Ctrl Pts',(-24.4674367735109,26.6397712546686,19.558783184522));
#50331=CARTESIAN_POINT('Ctrl Pts',(-24.4527209399813,26.644101854464,19.5578336431804));
#50332=CARTESIAN_POINT('Ctrl Pts',(-24.1998127643054,26.7165701723658,19.5414887879166));
#50333=CARTESIAN_POINT('Ctrl Pts',(-23.9546286125756,26.7571086681741,19.5251505746842));
#50334=CARTESIAN_POINT('Ctrl Pts',(-23.5522376874651,26.7767378965417,19.4979461876095));
#50335=CARTESIAN_POINT('Ctrl Pts',(-23.3968522552404,26.7730901752822,19.4873734420729));
#50336=CARTESIAN_POINT('Ctrl Pts',(-23.1449115386135,26.7489076212686,19.4705785628578));
#50337=CARTESIAN_POINT('Ctrl Pts',(-23.0479560850018,26.735122760423,19.4642040814213));
#50338=CARTESIAN_POINT('Ctrl Pts',(-22.9450585744924,26.7156757999477,19.457636985126));
#50339=CARTESIAN_POINT('Ctrl Pts',(-22.9383526754118,26.714386340645,19.457209916703));
#50340=CARTESIAN_POINT('Ctrl Pts',(-22.9295754519718,26.7126696448002,19.4566521778557));
#50341=CARTESIAN_POINT('Ctrl Pts',(-22.9275004440197,26.7122616828379,19.4565204148608));
#50342=CARTESIAN_POINT('Ctrl Pts',(-22.9234102751695,26.7114533429485,19.4562608707779));
#50343=CARTESIAN_POINT('Ctrl Pts',(-22.9213950929089,26.7110530798751,19.4561330831635));
#50344=CARTESIAN_POINT('Ctrl Pts',(-22.9175315401428,26.7102818453892,19.4558882545023));
#50345=CARTESIAN_POINT('Ctrl Pts',(-22.9156831180002,26.7099111803112,19.4557711965168));
#50346=CARTESIAN_POINT('Ctrl Pts',(-22.9114396690411,26.7090563653522,19.4555026337744));
#50347=CARTESIAN_POINT('Ctrl Pts',(-22.9090448612226,26.7085711122758,19.4553511927897));
#50348=CARTESIAN_POINT('Ctrl Pts',(-22.9014707621504,26.7070274244021,19.4548726119676));
#50349=CARTESIAN_POINT('Ctrl Pts',(-22.8962934879563,26.7059589625554,19.4545460465987));
#50350=CARTESIAN_POINT('Ctrl Pts',(-22.8529926226232,26.6969115930808,19.4518193522959));
#50351=CARTESIAN_POINT('Ctrl Pts',(-22.8150118692957,26.6882544645851,19.4494574034476));
#50352=CARTESIAN_POINT('Ctrl Pts',(-22.6169125669422,26.6393062916057,19.4372498471567));
#50353=CARTESIAN_POINT('Ctrl Pts',(-22.4598900640844,26.5874386098432,19.4279513984257));
#50354=CARTESIAN_POINT('Ctrl Pts',(-22.2285849796288,26.4907680364883,19.4139211743695));
#50355=CARTESIAN_POINT('Ctrl Pts',(-22.1510304824955,26.4546631934723,19.4091577064034));
#50356=CARTESIAN_POINT('Ctrl Pts',(-22.0750358228142,26.4155366754296,19.4043601800006));
#50357=CARTESIAN_POINT('Ctrl Pts',(-22.0750360918396,26.4155368139396,19.1544452962233));
#50358=CARTESIAN_POINT('Ctrl Pts',(-22.1221684381613,26.4398033108361,19.1575725024168));
#50359=CARTESIAN_POINT('Ctrl Pts',(-22.1699019589603,26.4629081104642,19.1607367299289));
#50360=CARTESIAN_POINT('Ctrl Pts',(-22.2311167606217,26.4906946378061,19.1648005015267));
#50361=CARTESIAN_POINT('Ctrl Pts',(-22.2440777421048,26.4964749216358,19.1656612367655));
#50362=CARTESIAN_POINT('Ctrl Pts',(-22.2667773444303,26.5064191672319,19.1671694570337));
#50363=CARTESIAN_POINT('Ctrl Pts',(-22.2764991666115,26.5106211057269,19.1678156369838));
#50364=CARTESIAN_POINT('Ctrl Pts',(-22.2905103687364,26.5165951926559,19.1687473200759));
#50365=CARTESIAN_POINT('Ctrl Pts',(-22.2947832119106,26.5184061473449,19.1690314986718));
#50366=CARTESIAN_POINT('Ctrl Pts',(-22.3022075366949,26.5215338914312,19.1695253746352));
#50367=CARTESIAN_POINT('Ctrl Pts',(-22.3053572355772,26.522854915099,19.169734927461));
#50368=CARTESIAN_POINT('Ctrl Pts',(-22.3114188786681,26.5253859213306,19.1701382764341));
#50369=CARTESIAN_POINT('Ctrl Pts',(-22.3143305119638,26.5265966426845,19.1703320471834));
#50370=CARTESIAN_POINT('Ctrl Pts',(-22.3211958694961,26.5294395986256,19.1707890067172));
#50371=CARTESIAN_POINT('Ctrl Pts',(-22.3251510689515,26.5310682362249,19.1710523173265));
#50372=CARTESIAN_POINT('Ctrl Pts',(-22.3368472582525,26.5358571799129,19.1718311307625));
#50373=CARTESIAN_POINT('Ctrl Pts',(-22.3445972732346,26.5389952219764,19.1723473870162));
#50374=CARTESIAN_POINT('Ctrl Pts',(-22.4129474566528,26.5663616355136,19.1769023961048));
#50375=CARTESIAN_POINT('Ctrl Pts',(-22.4742545484936,26.5887726144032,19.1810020445709));
#50376=CARTESIAN_POINT('Ctrl Pts',(-22.5559465616559,26.6158529850348,19.1864889905916));
#50377=CARTESIAN_POINT('Ctrl Pts',(-22.5757594394291,26.6222085344844,19.1878215451431));
#50378=CARTESIAN_POINT('Ctrl Pts',(-22.6197713040256,26.6358579816365,19.1907856651333));
#50379=CARTESIAN_POINT('Ctrl Pts',(-22.6439971898261,26.6430599147796,19.1924199049347));
#50380=CARTESIAN_POINT('Ctrl Pts',(-22.8919476578913,26.7136079364999,19.2091725434781));
#50381=CARTESIAN_POINT('Ctrl Pts',(-23.1217985524594,26.7528426763249,19.2249927352846));
#50382=CARTESIAN_POINT('Ctrl Pts',(-23.5143236361743,26.7768112620511,19.2515346001324));
#50383=CARTESIAN_POINT('Ctrl Pts',(-23.6753494629523,26.7745876123904,19.2622670309256));
#50384=CARTESIAN_POINT('Ctrl Pts',(-23.8461464369167,26.7594077841469,19.2730621890972));
#50385=CARTESIAN_POINT('Ctrl Pts',(-23.856733812609,26.7584139786132,19.273728891487));
#50386=CARTESIAN_POINT('Ctrl Pts',(-23.8705523789893,26.7570478393502,19.2745956702543));
#50387=CARTESIAN_POINT('Ctrl Pts',(-23.8737880381372,26.7567230077279,19.2747983857727));
#50388=CARTESIAN_POINT('Ctrl Pts',(-23.8790673704782,26.7561849368245,19.2751287350096));
#50389=CARTESIAN_POINT('Ctrl Pts',(-23.8811113310427,26.7559746405832,19.2752565352198));
#50390=CARTESIAN_POINT('Ctrl Pts',(-23.8850303136261,26.7555676415691,19.2755013815332));
#50391=CARTESIAN_POINT('Ctrl Pts',(-23.8869053584619,26.7553712488577,19.2756184445885));
#50392=CARTESIAN_POINT('Ctrl Pts',(-23.8912101482216,26.7549165447518,19.2758870102717));
#50393=CARTESIAN_POINT('Ctrl Pts',(-23.8936397781588,26.7546571147509,19.2760384491387));
#50394=CARTESIAN_POINT('Ctrl Pts',(-23.9013243076711,26.7538277390682,19.2765169896524));
#50395=CARTESIAN_POINT('Ctrl Pts',(-23.9065781359438,26.7532476247106,19.2768435169965));
#50396=CARTESIAN_POINT('Ctrl Pts',(-23.9505128715198,26.7482870249172,19.2795688534602));
#50397=CARTESIAN_POINT('Ctrl Pts',(-23.9891150081016,26.7432187104726,19.2819295250954));
#50398=CARTESIAN_POINT('Ctrl Pts',(-24.2415425939763,26.7054111634755,19.2971994977883));
#50399=CARTESIAN_POINT('Ctrl Pts',(-24.4517273585479,26.6519095192429,19.3091514917754));
#50400=CARTESIAN_POINT('Ctrl Pts',(-24.7930242195584,26.527369874711,19.329463976096));
#50401=CARTESIAN_POINT('Ctrl Pts',(-24.9274482323011,26.4676206565251,19.3377172356267));
#50402=CARTESIAN_POINT('Ctrl Pts',(-25.1175670466377,26.3670394423618,19.3501912124659));
#50403=CARTESIAN_POINT('Ctrl Pts',(-25.176785098103,26.3332642386176,19.3541967624321));
#50404=CARTESIAN_POINT('Ctrl Pts',(-25.2724362956922,26.274613174753,19.3608992083727));
#50405=CARTESIAN_POINT('Ctrl Pts',(-25.3095099823458,26.2508211311688,19.3635570334656));
#50406=CARTESIAN_POINT('Ctrl Pts',(-25.3524523707585,26.2220032948189,19.3667112388306));
#50407=CARTESIAN_POINT('Ctrl Pts',(-25.3588063409578,26.217706283416,19.3671799287843));
#50408=CARTESIAN_POINT('Ctrl Pts',(-25.3685070153102,26.2110953961325,19.3678985411106));
#50409=CARTESIAN_POINT('Ctrl Pts',(-25.3718648093741,26.2087977778744,19.368147845381));
#50410=CARTESIAN_POINT('Ctrl Pts',(-25.3779742313419,26.2046003107227,19.3686024803885));
#50411=CARTESIAN_POINT('Ctrl Pts',(-25.3807272744784,26.2027025235491,19.3688077323191));
#50412=CARTESIAN_POINT('Ctrl Pts',(-25.3862513430826,26.1988818570536,19.3692203496874));
#50413=CARTESIAN_POINT('Ctrl Pts',(-25.3890223132415,26.1969589054547,19.3694277177221));
#50414=CARTESIAN_POINT('Ctrl Pts',(-25.3968850818184,26.1914841249653,19.3700172528225));
#50415=CARTESIAN_POINT('Ctrl Pts',(-25.4019696223125,26.1879219423522,19.3703998164226));
#50416=CARTESIAN_POINT('Ctrl Pts',(-25.4234008895915,26.1728148840466,19.3720179943156));
#50417=CARTESIAN_POINT('Ctrl Pts',(-25.4396499087571,26.1611327635552,19.3732588855011));
#50418=CARTESIAN_POINT('Ctrl Pts',(-25.4596399902921,26.1464766937902,19.3748031749391));
#50419=CARTESIAN_POINT('Ctrl Pts',(-25.46348490088,26.1436445707051,19.3751010242227));
#50420=CARTESIAN_POINT('Ctrl Pts',(-25.4767365107887,26.1338380574963,19.37613041216));
#50421=CARTESIAN_POINT('Ctrl Pts',(-25.4861113970156,26.126821012941,19.3768636120134));
#50422=CARTESIAN_POINT('Ctrl Pts',(-25.4992549830674,26.1168708923668,19.37789860532));
#50423=CARTESIAN_POINT('Ctrl Pts',(-25.5030558061851,26.1139802347747,19.378198737437));
#50424=CARTESIAN_POINT('Ctrl Pts',(-25.7629431667796,25.9154136486053,19.3987782124467));
#50425=CARTESIAN_POINT('Ctrl Pts',(-25.9881914708585,25.6824682780081,19.4207202399));
#50426=CARTESIAN_POINT('Ctrl Pts',(-26.2567280121358,25.3055027570072,19.4518888945861));
#50427=CARTESIAN_POINT('Ctrl Pts',(-26.3307787988262,25.1856718639464,19.4612409598152));
#50428=CARTESIAN_POINT('Ctrl Pts',(-26.404161828062,25.0474392492601,19.4711390827669));
#50429=CARTESIAN_POINT('Ctrl Pts',(-26.4114552908466,25.033453507432,19.4721307653669));
#50430=CARTESIAN_POINT('Ctrl Pts',(-26.4203523494708,25.0160828798621,19.4733498958589));
#50431=CARTESIAN_POINT('Ctrl Pts',(-26.4220529483252,25.0127483234791,19.4735833568619));
#50432=CARTESIAN_POINT('Ctrl Pts',(-26.4247210457587,25.0074940851889,19.4739503147396));
#50433=CARTESIAN_POINT('Ctrl Pts',(-26.4256924330077,25.005576398598,19.4740840572156));
#50434=CARTESIAN_POINT('Ctrl Pts',(-26.4275037960429,25.0019915610038,19.4743337136073));
#50435=CARTESIAN_POINT('Ctrl Pts',(-26.4283442364047,25.0003246632521,19.4744496564478));
#50436=CARTESIAN_POINT('Ctrl Pts',(-26.430226898428,24.9965825777111,19.4747096195221));
#50437=CARTESIAN_POINT('Ctrl Pts',(-26.4312683235059,24.9945069976658,19.4748535888132));
#50438=CARTESIAN_POINT('Ctrl Pts',(-26.4339079191944,24.9892320169122,19.4752189217445));
#50439=CARTESIAN_POINT('Ctrl Pts',(-26.4355030139769,24.986031068763,19.4754400915411));
#50440=CARTESIAN_POINT('Ctrl Pts',(-26.4442432846729,24.9684181922014,19.4766542320184));
#50441=CARTESIAN_POINT('Ctrl Pts',(-26.4512859755424,24.9539552430897,19.4776408544205));
#50442=CARTESIAN_POINT('Ctrl Pts',(-26.5936168007394,24.6560159732322,19.497765497533));
#50443=CARTESIAN_POINT('Ctrl Pts',(-26.6868774443053,24.3542676692754,19.5145701044672));
#50444=CARTESIAN_POINT('Ctrl Pts',(-26.7602784156923,23.8805777174499,19.5416913708803));
#50445=CARTESIAN_POINT('Ctrl Pts',(-26.7729823325598,23.7157290758983,19.5512353328095));
#50446=CARTESIAN_POINT('Ctrl Pts',(-26.7730053753846,23.5271809363017,19.5626176023256));
#50447=CARTESIAN_POINT('Ctrl Pts',(-26.7727519586169,23.503716649047,19.5640419645022));
#50448=CARTESIAN_POINT('Ctrl Pts',(-26.7721006155328,23.4737341420675,19.5658727087148));
#50449=CARTESIAN_POINT('Ctrl Pts',(-26.7719390861145,23.4672110759976,19.5662716570329));
#50450=CARTESIAN_POINT('Ctrl Pts',(-26.7716505731733,23.4568336198899,19.5669073833977));
#50451=CARTESIAN_POINT('Ctrl Pts',(-26.771536478879,23.4529788655141,19.5671437563493));
#50452=CARTESIAN_POINT('Ctrl Pts',(-26.7713209926038,23.4461151375993,19.5675650510075));
#50453=CARTESIAN_POINT('Ctrl Pts',(-26.7712223024683,23.4431060787663,19.5677498876086));
#50454=CARTESIAN_POINT('Ctrl Pts',(-26.7709843500903,23.4361485151568,19.5681775959124));
#50455=CARTESIAN_POINT('Ctrl Pts',(-26.7708420432158,23.4322001252137,19.5684205630126));
#50456=CARTESIAN_POINT('Ctrl Pts',(-26.7704227503542,23.4211320774625,19.5691023337704));
#50457=CARTESIAN_POINT('Ctrl Pts',(-26.7701294149431,23.4140130944565,19.5695416504755));
#50458=CARTESIAN_POINT('Ctrl Pts',(-26.7682957071976,23.3728311649924,19.5720877061208));
#50459=CARTESIAN_POINT('Ctrl Pts',(-26.7662384713044,23.3387944675573,19.574210629688));
#50460=CARTESIAN_POINT('Ctrl Pts',(-26.758744417175,23.2406854771148,19.5803861495505));
#50461=CARTESIAN_POINT('Ctrl Pts',(-26.7519298902201,23.1767380245799,19.5844811522186));
#50462=CARTESIAN_POINT('Ctrl Pts',(-26.7324550949608,23.03451373876,19.5937487862557));
#50463=CARTESIAN_POINT('Ctrl Pts',(-26.7188098773828,22.9564154519873,19.5989475356285));
#50464=CARTESIAN_POINT('Ctrl Pts',(-26.640513763091,22.5888073664287,19.6239019810644));
#50465=CARTESIAN_POINT('Ctrl Pts',(-26.5389826579718,22.3086518958653,19.6445200722151));
#50466=CARTESIAN_POINT('Ctrl Pts',(-26.3982318458674,22.0418902706163,19.6639646380911));
#50467=CARTESIAN_POINT('Ctrl Pts',(-26.3958731529694,22.0374451529986,19.6642885457887));
#50468=CARTESIAN_POINT('Ctrl Pts',(-26.3763375012322,22.0008362343624,19.6669552187952));
#50469=CARTESIAN_POINT('Ctrl Pts',(-26.358625312654,21.9689588456189,19.6692711804535));
#50470=CARTESIAN_POINT('Ctrl Pts',(-26.3380375357719,21.9333437068122,19.6718459405409));
#50471=CARTESIAN_POINT('Ctrl Pts',(-26.3356912742873,21.9293051578241,19.6721377157322));
#50472=CARTESIAN_POINT('Ctrl Pts',(-26.3321339688191,21.9232126066965,19.6725775869626));
#50473=CARTESIAN_POINT('Ctrl Pts',(-26.3309294240693,21.921154846453,19.6727261016302));
#50474=CARTESIAN_POINT('Ctrl Pts',(-26.3288340028151,21.9175842698979,19.6729837079539));
#50475=CARTESIAN_POINT('Ctrl Pts',(-26.3279441739946,21.9160708450198,19.6730928680008));
#50476=CARTESIAN_POINT('Ctrl Pts',(-26.3260821660831,21.9129098482735,19.6733208019718));
#50477=CARTESIAN_POINT('Ctrl Pts',(-26.3251097574168,21.9112624161112,19.673439560121));
#50478=CARTESIAN_POINT('Ctrl Pts',(-26.3227860944382,21.9073337156819,19.673722685608));
#50479=CARTESIAN_POINT('Ctrl Pts',(-26.3214334866078,21.9050532404853,19.6738869641445));
#50480=CARTESIAN_POINT('Ctrl Pts',(-26.3168654170688,21.8973731653502,19.6744399998086));
#50481=CARTESIAN_POINT('Ctrl Pts',(-26.3136369498494,21.8919812582657,19.6748279099213));
#50482=CARTESIAN_POINT('Ctrl Pts',(-26.2496409394764,21.7858065460386,19.6824601002862));
#50483=CARTESIAN_POINT('Ctrl Pts',(-26.1834055976511,21.6884041134285,19.6893497353751));
#50484=CARTESIAN_POINT('Ctrl Pts',(-25.9012697710289,21.3187875975391,19.7159468684082));
#50485=CARTESIAN_POINT('Ctrl Pts',(-25.6473419314238,21.0786227451493,19.7345418995362));
#50486=CARTESIAN_POINT('Ctrl Pts',(-25.3581568800172,20.8823686867559,19.7553762604681));
#50487=CARTESIAN_POINT('Ctrl Pts',(-25.3563465179536,20.8811427820714,19.7555066637219));
#50488=CARTESIAN_POINT('Ctrl Pts',(-25.343642361796,20.8725588795465,19.7564215967776));
#50489=CARTESIAN_POINT('Ctrl Pts',(-25.3327050015424,20.8652658347717,19.7572084259371));
#50490=CARTESIAN_POINT('Ctrl Pts',(-25.3114134142272,20.8512560093806,19.75873868261));
#50491=CARTESIAN_POINT('Ctrl Pts',(-25.3010646095662,20.8445313813898,19.7594818087199));
#50492=CARTESIAN_POINT('Ctrl Pts',(-25.2714667477881,20.8255396681928,19.7616055420286));
#50493=CARTESIAN_POINT('Ctrl Pts',(-25.2521259344205,20.8134175995629,19.7629913605956));
#50494=CARTESIAN_POINT('Ctrl Pts',(-25.2270856955448,20.798091418781,19.7647836729528));
#50495=CARTESIAN_POINT('Ctrl Pts',(-25.2215027003002,20.7946975742015,19.7651831687931));
#50496=CARTESIAN_POINT('Ctrl Pts',(-25.2126389454609,20.7893462368768,19.7658172477574));
#50497=CARTESIAN_POINT('Ctrl Pts',(-25.2093649383193,20.7873775472944,19.7660514200929));
#50498=CARTESIAN_POINT('Ctrl Pts',(-25.2032421028685,20.7837106397512,19.7664892873017));
#50499=CARTESIAN_POINT('Ctrl Pts',(-25.2003941359271,20.7820109872954,19.7666929293568));
#50500=CARTESIAN_POINT('Ctrl Pts',(-25.1939951118856,20.7782054654818,19.7671504297941));
#50501=CARTESIAN_POINT('Ctrl Pts',(-25.1904426264056,20.7761020202424,19.767404376192));
#50502=CARTESIAN_POINT('Ctrl Pts',(-25.1806362418608,20.7703210296929,19.7681052735706));
#50503=CARTESIAN_POINT('Ctrl Pts',(-25.1743739795188,20.7666577839746,19.7685527439357));
#50504=CARTESIAN_POINT('Ctrl Pts',(-25.1600407254038,20.7583380707227,19.7695766881891));
#50505=CARTESIAN_POINT('Ctrl Pts',(-25.151961829298,20.7536954146261,19.7701536589006));
#50506=CARTESIAN_POINT('Ctrl Pts',(-24.9730071160529,20.6518862965419,19.7829307351051));
#50507=CARTESIAN_POINT('Ctrl Pts',(-24.7936498200508,20.5705386269109,19.7957091504999));
#50508=CARTESIAN_POINT('Ctrl Pts',(-24.3538006150174,20.4177032833967,19.8268598330285));
#50509=CARTESIAN_POINT('Ctrl Pts',(-24.0895115242429,20.3615605207254,19.8454755720337));
#50510=CARTESIAN_POINT('Ctrl Pts',(-23.8158369890735,20.3384597720983,19.8631654151476));
#50511=CARTESIAN_POINT('Ctrl Pts',(-23.810353261897,20.3380110330498,19.8635191898669));
#50512=CARTESIAN_POINT('Ctrl Pts',(-23.7703328973437,20.3348392789799,19.8660959299755));
#50513=CARTESIAN_POINT('Ctrl Pts',(-23.73575375873,20.3326591313163,19.8682945563317));
#50514=CARTESIAN_POINT('Ctrl Pts',(-23.696548532263,20.3308214931447,19.8707508326875));
#50515=CARTESIAN_POINT('Ctrl Pts',(-23.6919520819407,20.3306159109181,19.8710382406109));
#50516=CARTESIAN_POINT('Ctrl Pts',(-23.6849908452259,20.3303194967462,19.8714726385841));
#50517=CARTESIAN_POINT('Ctrl Pts',(-23.6826263976341,20.3302214258837,19.8716200328316));
#50518=CARTESIAN_POINT('Ctrl Pts',(-23.6785121752119,20.3300553183786,19.8718762353191));
#50519=CARTESIAN_POINT('Ctrl Pts',(-23.67676245317,20.3299861034925,19.8719851101476));
#50520=CARTESIAN_POINT('Ctrl Pts',(-23.6730971532589,20.3298441047758,19.8722130016775));
#50521=CARTESIAN_POINT('Ctrl Pts',(-23.67118156776,20.3297716040263,19.8723320018219));
#50522=CARTESIAN_POINT('Ctrl Pts',(-23.6665951046673,20.329602114281,19.8726166801285));
#50523=CARTESIAN_POINT('Ctrl Pts',(-23.6639241609116,20.3295067382009,19.8727822669157));
#50524=CARTESIAN_POINT('Ctrl Pts',(-23.6552740239779,20.3292086263199,19.8733179094199));
#50525=CARTESIAN_POINT('Ctrl Pts',(-23.6492943389985,20.3290192157176,19.8736872178646));
#50526=CARTESIAN_POINT('Ctrl Pts',(-23.6349953446451,20.328606139293,19.8745680818306));
#50527=CARTESIAN_POINT('Ctrl Pts',(-23.6266755794775,20.3283980434681,19.8750787859253));
#50528=CARTESIAN_POINT('Ctrl Pts',(-23.3231260499265,20.32198206696,19.8936486340493));
#50529=CARTESIAN_POINT('Ctrl Pts',(-23.0283825337816,20.3563463589111,19.9095827325815));
#50530=CARTESIAN_POINT('Ctrl Pts',(-22.5466903300657,20.4810747204834,19.9375864837191));
#50531=CARTESIAN_POINT('Ctrl Pts',(-22.356211274837,20.5500464758041,19.9492093617702));
#50532=CARTESIAN_POINT('Ctrl Pts',(-22.162075288751,20.6417752478567,19.9622569094588));
#50533=CARTESIAN_POINT('Ctrl Pts',(-22.1507202607469,20.6472221178088,19.9630244786));
#50534=CARTESIAN_POINT('Ctrl Pts',(-22.135244909394,20.6547573539238,19.9640767235219));
#50535=CARTESIAN_POINT('Ctrl Pts',(-22.131096612386,20.6567882806639,19.9643593937625));
#50536=CARTESIAN_POINT('Ctrl Pts',(-22.124042212541,20.6602607995865,19.9648411299618));
#50537=CARTESIAN_POINT('Ctrl Pts',(-22.1211338853,20.6616978791867,19.9650400378205));
#50538=CARTESIAN_POINT('Ctrl Pts',(-22.1155116134188,20.6644865584628,19.9654251456702));
#50539=CARTESIAN_POINT('Ctrl Pts',(-22.1127973960015,20.6658376018329,19.9656113259712));
#50540=CARTESIAN_POINT('Ctrl Pts',(-22.1063593633346,20.6690535754149,19.9660535709041));
#50541=CARTESIAN_POINT('Ctrl Pts',(-22.102637255469,20.6709218943619,19.9663097543792));
#50542=CARTESIAN_POINT('Ctrl Pts',(-22.0918072557449,20.6763843406391,19.9670566273743));
#50543=CARTESIAN_POINT('Ctrl Pts',(-22.0847090916876,20.6799975907308,19.9675479896227));
#50544=CARTESIAN_POINT('Ctrl Pts',(-22.0354514188585,20.7053020774889,19.9709707753497));
#50545=CARTESIAN_POINT('Ctrl Pts',(-21.9937635636994,20.7278940846513,19.973933964329));
#50546=CARTESIAN_POINT('Ctrl Pts',(-21.8627109358804,20.8027024162582,19.9834696659796));
#50547=CARTESIAN_POINT('Ctrl Pts',(-21.7753633092832,20.8583029092912,19.9901618560945));
#50548=CARTESIAN_POINT('Ctrl Pts',(-21.5096593793589,21.0459945083397,20.011591176318));
#50549=CARTESIAN_POINT('Ctrl Pts',(-21.3421788093365,21.1923459767152,20.0267643235587));
#50550=CARTESIAN_POINT('Ctrl Pts',(-21.0977106554621,21.4550348037051,20.0508675102469));
#50551=CARTESIAN_POINT('Ctrl Pts',(-21.0108278513863,21.5612248040067,20.0599288595187));
#50552=CARTESIAN_POINT('Ctrl Pts',(-20.9262936562505,21.6791508259306,20.069040880182));
#50553=CARTESIAN_POINT('Ctrl Pts',(-20.921649332455,21.6856809998023,20.0695425177494));
#50554=CARTESIAN_POINT('Ctrl Pts',(-20.9154611523959,21.6944509936076,20.0702122089207));
#50555=CARTESIAN_POINT('Ctrl Pts',(-20.9138957574328,21.6966754709474,20.0703817300026));
#50556=CARTESIAN_POINT('Ctrl Pts',(-20.9112722856753,21.7004135565131,20.0706660186533));
#50557=CARTESIAN_POINT('Ctrl Pts',(-20.9102126939653,21.7019260918515,20.070780890745));
#50558=CARTESIAN_POINT('Ctrl Pts',(-20.9081894902481,21.7048194435807,20.0710003259035));
#50559=CARTESIAN_POINT('Ctrl Pts',(-20.9072256662455,21.7062000958305,20.0711049032782));
#50560=CARTESIAN_POINT('Ctrl Pts',(-20.9049595853342,21.7094516227353,20.0713508779354));
#50561=CARTESIAN_POINT('Ctrl Pts',(-20.9036582326742,21.7113231216956,20.0714922123503));
#50562=CARTESIAN_POINT('Ctrl Pts',(-20.8999339880381,21.7166911676228,20.0718969139673));
#50563=CARTESIAN_POINT('Ctrl Pts',(-20.8975160203309,21.7201911500907,20.0721599431113));
#50564=CARTESIAN_POINT('Ctrl Pts',(-20.881360425045,21.7436754973192,20.0739192981064));
#50565=CARTESIAN_POINT('Ctrl Pts',(-20.8678413342444,21.7638102822884,20.0754009323319));
#50566=CARTESIAN_POINT('Ctrl Pts',(-20.82667936833,21.8266362151061,20.0799480632555));
#50567=CARTESIAN_POINT('Ctrl Pts',(-20.7998175588995,21.8698323264605,20.0829674235431));
#50568=CARTESIAN_POINT('Ctrl Pts',(-20.7374681984873,21.9755991086126,20.09015120636));
#50569=CARTESIAN_POINT('Ctrl Pts',(-20.7030302768715,22.0387580218041,20.0942704244645));
#50570=CARTESIAN_POINT('Ctrl Pts',(-20.5797308110551,22.2840835684309,20.1098259223461));
#50571=CARTESIAN_POINT('Ctrl Pts',(-20.5060093991629,22.4733265249975,20.1209453317185));
#50572=CARTESIAN_POINT('Ctrl Pts',(-20.431458465614,22.7353257430847,20.1364458983841));
#50573=CARTESIAN_POINT('Ctrl Pts',(-20.4145537565109,22.8030079353775,20.1404558476725));
#50574=CARTESIAN_POINT('Ctrl Pts',(-20.3803645103059,22.9616213405645,20.149926155676));
#50575=CARTESIAN_POINT('Ctrl Pts',(-20.3647753543345,23.052849891687,20.1554287935116));
#50576=CARTESIAN_POINT('Ctrl Pts',(-20.3518464650915,23.154752114926,20.1616818059197));
#50577=CARTESIAN_POINT('Ctrl Pts',(-20.3506087239092,23.1648936780674,20.1623052624745));
#50578=CARTESIAN_POINT('Ctrl Pts',(-20.3489400661048,23.1791285644539,20.1631820108497));
#50579=CARTESIAN_POINT('Ctrl Pts',(-20.3484687258045,23.1832171635281,20.1634340250008));
#50580=CARTESIAN_POINT('Ctrl Pts',(-20.3476195150417,23.1907096932295,20.1638962058187));
#50581=CARTESIAN_POINT('Ctrl Pts',(-20.3472392355953,23.1941133497434,20.1641062961199));
#50582=CARTESIAN_POINT('Ctrl Pts',(-20.346480683599,23.2010021952454,20.164531782781));
#50583=CARTESIAN_POINT('Ctrl Pts',(-20.3461026708638,23.2044874071619,20.1647471870109));
#50584=CARTESIAN_POINT('Ctrl Pts',(-20.3453571360882,23.2114673286247,20.1651788685839));
#50585=CARTESIAN_POINT('Ctrl Pts',(-20.3449896416838,23.2149620362115,20.1653951464871));
#50586=CARTESIAN_POINT('Ctrl Pts',(-20.3436633612314,23.2277758360225,20.1661886884369));
#50587=CARTESIAN_POINT('Ctrl Pts',(-20.3427395027563,23.2370984264986,20.1667670536321));
#50588=CARTESIAN_POINT('Ctrl Pts',(-20.3345237838355,23.3238557621488,20.1721591850645));
#50589=CARTESIAN_POINT('Ctrl Pts',(-20.3299972583153,23.4015207178485,20.1770596360268));
#50590=CARTESIAN_POINT('Ctrl Pts',(-20.3266525377133,23.5533372312413,20.1867945918078));
#50591=CARTESIAN_POINT('Ctrl Pts',(-20.3275754000759,23.6274355780089,20.1916182394667));
#50592=CARTESIAN_POINT('Ctrl Pts',(-20.3394530511492,23.8803571235831,20.2083152429478));
#50593=CARTESIAN_POINT('Ctrl Pts',(-20.3627578147318,24.0582587728889,20.2204787370895));
#50594=CARTESIAN_POINT('Ctrl Pts',(-20.4327290048486,24.3809030269292,20.2427930836691));
#50595=CARTESIAN_POINT('Ctrl Pts',(-20.4750845141968,24.5261032114347,20.2529267256994));
#50596=CARTESIAN_POINT('Ctrl Pts',(-20.5282528740876,24.669913491748,20.2627358800894));
#50597=CARTESIAN_POINT('Ctrl Pts',(-20.5290330741311,24.6720170280783,20.2628793076616));
#50598=CARTESIAN_POINT('Ctrl Pts',(-20.5395737845785,24.7003455991233,20.264810139642));
#50599=CARTESIAN_POINT('Ctrl Pts',(-20.5496736650995,24.7264443433088,20.2665806331491));
#50600=CARTESIAN_POINT('Ctrl Pts',(-20.5618767873656,24.7567973258967,20.268627148015));
#50601=CARTESIAN_POINT('Ctrl Pts',(-20.5636506276377,24.7611815127145,20.2689224376951));
#50602=CARTESIAN_POINT('Ctrl Pts',(-20.5663364092402,24.7677778339064,20.2693662387598));
#50603=CARTESIAN_POINT('Ctrl Pts',(-20.5672411636836,24.7699928588856,20.2695151836221));
#50604=CARTESIAN_POINT('Ctrl Pts',(-20.5688586858143,24.7739403217712,20.2697804734307));
#50605=CARTESIAN_POINT('Ctrl Pts',(-20.5695704965715,24.7756731441364,20.2698968765268));
#50606=CARTESIAN_POINT('Ctrl Pts',(-20.5710846828366,24.7793501333349,20.2701437698795));
#50607=CARTESIAN_POINT('Ctrl Pts',(-20.5718874486279,24.7812941305275,20.2702742355541));
#50608=CARTESIAN_POINT('Ctrl Pts',(-20.5735278516248,24.7852555734926,20.2705399662989));
#50609=CARTESIAN_POINT('Ctrl Pts',(-20.5743656382996,24.7872729567382,20.2706752221589));
#50610=CARTESIAN_POINT('Ctrl Pts',(-20.5780851993441,24.7962039809633,20.2712737064504));
#50611=CARTESIAN_POINT('Ctrl Pts',(-20.5809890510276,24.803108489278,20.2717355987693));
#50612=CARTESIAN_POINT('Ctrl Pts',(-20.6098847715482,24.8711492739382,20.2762801124419));
#50613=CARTESIAN_POINT('Ctrl Pts',(-20.6377392441712,24.9314833644604,20.2802522746689));
#50614=CARTESIAN_POINT('Ctrl Pts',(-20.6970417829515,25.0501493669342,20.2880320052594));
#50615=CARTESIAN_POINT('Ctrl Pts',(-20.7284622767839,25.108457515148,20.29183823175));
#50616=CARTESIAN_POINT('Ctrl Pts',(-20.8459079131071,25.311185393177,20.3051542435726));
#50617=CARTESIAN_POINT('Ctrl Pts',(-20.9414059160023,25.4498016839362,20.3144241374528));
#50618=CARTESIAN_POINT('Ctrl Pts',(-21.1750143140624,25.7378261411087,20.3352932122986));
#50619=CARTESIAN_POINT('Ctrl Pts',(-21.3173030170811,25.8828803648416,20.346948684621));
#50620=CARTESIAN_POINT('Ctrl Pts',(-21.4818793559255,26.0217112784928,20.3600325517818));
#50621=CARTESIAN_POINT('Ctrl Pts',(-21.4915457702573,26.0297690964178,20.3607995501883));
#50622=CARTESIAN_POINT('Ctrl Pts',(-21.5048229623825,26.0407056549606,20.3618511323362));
#50623=CARTESIAN_POINT('Ctrl Pts',(-21.5083931900323,26.043633631869,20.3621337138052));
#50624=CARTESIAN_POINT('Ctrl Pts',(-21.514482143933,26.0486053914465,20.3626153367678));
#50625=CARTESIAN_POINT('Ctrl Pts',(-21.5169976935598,26.0506530689293,20.3628142203202));
#50626=CARTESIAN_POINT('Ctrl Pts',(-21.5218706589228,26.0546074853283,20.3631993115273));
#50627=CARTESIAN_POINT('Ctrl Pts',(-21.5242276830347,26.056514702357,20.3633854995411));
#50628=CARTESIAN_POINT('Ctrl Pts',(-21.5298293836071,26.0610343258377,20.3638278101826));
#50629=CARTESIAN_POINT('Ctrl Pts',(-21.5330764346591,26.0636437683343,20.3640840517568));
#50630=CARTESIAN_POINT('Ctrl Pts',(-21.5425501950049,26.0712270259358,20.3648312574925));
#50631=CARTESIAN_POINT('Ctrl Pts',(-21.5487902721732,26.0761840223029,20.3653228953021));
#50632=CARTESIAN_POINT('Ctrl Pts',(-21.5956245381427,26.1131057470584,20.3690090322622));
#50633=CARTESIAN_POINT('Ctrl Pts',(-21.6369617977468,26.1441116765048,20.3722414206852));
#50634=CARTESIAN_POINT('Ctrl Pts',(-21.7320652509628,26.2119355928824,20.3796371593369));
#50635=CARTESIAN_POINT('Ctrl Pts',(-21.7862373774116,26.2481426855665,20.3838217599413));
#50636=CARTESIAN_POINT('Ctrl Pts',(-21.9174781507999,26.330217061326,20.393894382062));
#50637=CARTESIAN_POINT('Ctrl Pts',(-21.9954043122551,26.3745377092206,20.3998249117356));
#50638=CARTESIAN_POINT('Ctrl Pts',(-22.0750362907684,26.4155369163599,20.4058188292237));
#50639=CARTESIAN_POINT('Origin',(-23.5502525316942,23.5502525316942,-77.3107734492734));
#50640=CARTESIAN_POINT('',(-22.0750357484432,26.415536637139,21.9049549578222));
#50641=CARTESIAN_POINT('',(-22.075036015355,26.4155367745608,21.6601868380444));
#50642=CARTESIAN_POINT('',(-22.0750360153461,26.4155367745563,-77.3107734492734));
#50643=CARTESIAN_POINT('Ctrl Pts',(-22.0750357484432,26.415536637139,21.9049549578222));
#50644=CARTESIAN_POINT('Ctrl Pts',(-22.0088770685692,26.3814742575228,21.8999718987017));
#50645=CARTESIAN_POINT('Ctrl Pts',(-21.9438937780695,26.3451182736942,21.8949460589944));
#50646=CARTESIAN_POINT('Ctrl Pts',(-21.7492298965475,26.2271700388232,21.8795449272302));
#50647=CARTESIAN_POINT('Ctrl Pts',(-21.6240713338848,26.1385725783133,21.8691464575743));
#50648=CARTESIAN_POINT('Ctrl Pts',(-21.4522955103917,25.9975906616431,21.8545440013663));
#50649=CARTESIAN_POINT('Ctrl Pts',(-21.4003261726026,25.9520655740068,21.8500790058873));
#50650=CARTESIAN_POINT('Ctrl Pts',(-21.3417756085546,25.8973506447596,21.845032046154));
#50651=CARTESIAN_POINT('Ctrl Pts',(-21.3337340360379,25.8897579579112,21.8443385068057));
#50652=CARTESIAN_POINT('Ctrl Pts',(-21.323338804554,25.8798412829584,21.8434416871175));
#50653=CARTESIAN_POINT('Ctrl Pts',(-21.3209495410501,25.8775549775061,21.8432355399513));
#50654=CARTESIAN_POINT('Ctrl Pts',(-21.3170833391493,25.8738439611435,21.8429019354042));
#50655=CARTESIAN_POINT('Ctrl Pts',(-21.3156042428099,25.8724215174885,21.8427743017775));
#50656=CARTESIAN_POINT('Ctrl Pts',(-21.3127683599552,25.8696890366998,21.8425295786826));
#50657=CARTESIAN_POINT('Ctrl Pts',(-21.3114113688423,25.8683792251839,21.842412472614));
#50658=CARTESIAN_POINT('Ctrl Pts',(-21.3082952005647,25.8653661107243,21.8421435410459));
#50659=CARTESIAN_POINT('Ctrl Pts',(-21.3065368100737,25.8636619894132,21.8419917799025));
#50660=CARTESIAN_POINT('Ctrl Pts',(-21.3009687201596,25.8582534273265,21.8415111818616));
#50661=CARTESIAN_POINT('Ctrl Pts',(-21.2971662144503,25.854541542881,21.8411829263497));
#50662=CARTESIAN_POINT('Ctrl Pts',(-21.2650690569451,25.8230539141596,21.8384114951209));
#50663=CARTESIAN_POINT('Ctrl Pts',(-21.2372784762305,25.7947660662278,21.8360078984496));
#50664=CARTESIAN_POINT('Ctrl Pts',(-21.0677861626997,25.6157486533297,21.8212673586743));
#50665=CARTESIAN_POINT('Ctrl Pts',(-20.9403324311978,25.4521602224927,21.8097994840551));
#50666=CARTESIAN_POINT('Ctrl Pts',(-20.7528924864414,25.1568918490335,21.7902540007185));
#50667=CARTESIAN_POINT('Ctrl Pts',(-20.6844553229816,25.0313723529527,21.7822526729934));
#50668=CARTESIAN_POINT('Ctrl Pts',(-20.5900289670077,24.8269587000176,21.7692581437212));
#50669=CARTESIAN_POINT('Ctrl Pts',(-20.5583687786117,24.7508907736037,21.7644318311119));
#50670=CARTESIAN_POINT('Ctrl Pts',(-20.5198901978335,24.6474338783318,21.7578337597834));
#50671=CARTESIAN_POINT('Ctrl Pts',(-20.5104650608245,24.6210442197741,21.7561479562325));
#50672=CARTESIAN_POINT('Ctrl Pts',(-20.4955296043008,24.5774389733186,21.7533562302207));
#50673=CARTESIAN_POINT('Ctrl Pts',(-20.4898177477939,24.5602936505351,21.7522569909421));
#50674=CARTESIAN_POINT('Ctrl Pts',(-20.4825476991702,24.5378431212792,21.7508153106236));
#50675=CARTESIAN_POINT('Ctrl Pts',(-20.4808584540624,24.5325804340391,21.7504771979234));
#50676=CARTESIAN_POINT('Ctrl Pts',(-20.4780762919761,24.5238356222411,21.7499150859459));
#50677=CARTESIAN_POINT('Ctrl Pts',(-20.4769757321614,24.5203559258572,21.7496913386986));
#50678=CARTESIAN_POINT('Ctrl Pts',(-20.4748722516965,24.5136657395236,21.7492610089146));
#50679=CARTESIAN_POINT('Ctrl Pts',(-20.4738684411419,24.5104555325638,21.7490544559785));
#50680=CARTESIAN_POINT('Ctrl Pts',(-20.4715939360499,24.5031414394652,21.7485836994924));
#50681=CARTESIAN_POINT('Ctrl Pts',(-20.4703264203127,24.4990365783731,21.748319391891));
#50682=CARTESIAN_POINT('Ctrl Pts',(-20.4664956077023,24.4865418866063,21.7475145404217));
#50683=CARTESIAN_POINT('Ctrl Pts',(-20.4639583724657,24.478144164732,21.746973142721));
#50684=CARTESIAN_POINT('Ctrl Pts',(-20.4461250823004,24.4182372704553,21.7431076001775));
#50685=CARTESIAN_POINT('Ctrl Pts',(-20.4320858357014,24.3663656498333,21.7397426037319));
#50686=CARTESIAN_POINT('Ctrl Pts',(-20.4149776543517,24.2962480506356,21.7351662565127));
#50687=CARTESIAN_POINT('Ctrl Pts',(-20.4107589248725,24.2782894408829,21.7339917634516));
#50688=CARTESIAN_POINT('Ctrl Pts',(-20.3475228100442,23.9983257138685,21.7156443340768));
#50689=CARTESIAN_POINT('Ctrl Pts',(-20.3213394005373,23.7300232487341,21.6974144067586));
#50690=CARTESIAN_POINT('Ctrl Pts',(-20.3334163008781,23.2909265648678,21.6677520103089));
#50691=CARTESIAN_POINT('Ctrl Pts',(-20.3516759376082,23.1208231680326,21.6563413863853));
#50692=CARTESIAN_POINT('Ctrl Pts',(-20.3844797145807,22.9468969458099,21.6452506482799));
#50693=CARTESIAN_POINT('Ctrl Pts',(-20.3856385311446,22.9408481326202,21.644865682947));
#50694=CARTESIAN_POINT('Ctrl Pts',(-20.3873168591515,22.9322214576985,21.6443177600331));
#50695=CARTESIAN_POINT('Ctrl Pts',(-20.3878221877036,22.9296409006454,21.6441539973687));
#50696=CARTESIAN_POINT('Ctrl Pts',(-20.3886998114812,22.9251880519513,21.6438716661104));
#50697=CARTESIAN_POINT('Ctrl Pts',(-20.3890706123262,22.9233154700552,21.6437530113181));
#50698=CARTESIAN_POINT('Ctrl Pts',(-20.3897865672665,22.9197166093846,21.6435251187672));
#50699=CARTESIAN_POINT('Ctrl Pts',(-20.3901314713808,22.9179902871866,21.643415866705));
#50700=CARTESIAN_POINT('Ctrl Pts',(-20.3909505885342,22.9139078368668,21.6431576559813));
#50701=CARTESIAN_POINT('Ctrl Pts',(-20.3914260238173,22.9115519508961,21.6430087679043));
#50702=CARTESIAN_POINT('Ctrl Pts',(-20.3928479760104,22.9045462900902,21.6425663706255));
#50703=CARTESIAN_POINT('Ctrl Pts',(-20.3938021326733,22.8998980453558,21.6422732980125));
#50704=CARTESIAN_POINT('Ctrl Pts',(-20.402597791818,22.857524683748,21.6396056824188));
#50705=CARTESIAN_POINT('Ctrl Pts',(-20.4111054261117,22.8199388968835,21.6372686294094));
#50706=CARTESIAN_POINT('Ctrl Pts',(-20.4597091592694,22.6217883278776,21.6250592180799));
#50707=CARTESIAN_POINT('Ctrl Pts',(-20.5114590835634,22.464319025119,21.6157387628019));
#50708=CARTESIAN_POINT('Ctrl Pts',(-20.6472401573578,22.1382055704558,21.5959687067993));
#50709=CARTESIAN_POINT('Ctrl Pts',(-20.7343954175306,21.9715500120746,21.5855609917238));
#50710=CARTESIAN_POINT('Ctrl Pts',(-20.8934796775097,21.7228973687797,21.5685105705931));
#50711=CARTESIAN_POINT('Ctrl Pts',(-20.9558888351996,21.63532637298,21.5621768312115));
#50712=CARTESIAN_POINT('Ctrl Pts',(-21.030197333126,21.5413744128405,21.5549235906861));
#50713=CARTESIAN_POINT('Ctrl Pts',(-21.0378991874546,21.5317505704931,21.554175042109));
#50714=CARTESIAN_POINT('Ctrl Pts',(-21.0497820876604,21.517075679911,21.5530249329338));
#50715=CARTESIAN_POINT('Ctrl Pts',(-21.0539237114035,21.5119927415542,21.5526249580603));
#50716=CARTESIAN_POINT('Ctrl Pts',(-21.0616365231719,21.5025857190596,21.5518817057441));
#50717=CARTESIAN_POINT('Ctrl Pts',(-21.0652035487046,21.4982582419964,21.5515385976982));
#50718=CARTESIAN_POINT('Ctrl Pts',(-21.0710664908655,21.4911830917973,21.5509756700158));
#50719=CARTESIAN_POINT('Ctrl Pts',(-21.0733557337106,21.4884298828391,21.5507561228822));
#50720=CARTESIAN_POINT('Ctrl Pts',(-21.0778165664352,21.4830831137278,21.5503288009968));
#50721=CARTESIAN_POINT('Ctrl Pts',(-21.0799876614808,21.480489145282,21.5501210466682));
#50722=CARTESIAN_POINT('Ctrl Pts',(-21.08496922953,21.4745562992279,21.5496448644687));
#50723=CARTESIAN_POINT('Ctrl Pts',(-21.0877824044507,21.4712197081104,21.5493763258121));
#50724=CARTESIAN_POINT('Ctrl Pts',(-21.0966509818181,21.4607443054288,21.5485309046173));
#50725=CARTESIAN_POINT('Ctrl Pts',(-21.1027306749654,21.4536262056518,21.5479530211095));
#50726=CARTESIAN_POINT('Ctrl Pts',(-21.1262269557873,21.4263582489577,21.5457260034582));
#50727=CARTESIAN_POINT('Ctrl Pts',(-21.143861678723,21.4063985462462,21.5440678168645));
#50728=CARTESIAN_POINT('Ctrl Pts',(-21.1658906469998,21.3820795302137,21.5420120308799));
#50729=CARTESIAN_POINT('Ctrl Pts',(-21.170053093519,21.3775108546454,21.5416242561158));
#50730=CARTESIAN_POINT('Ctrl Pts',(-21.1788530448962,21.3679077173373,21.5408058549723));
#50731=CARTESIAN_POINT('Ctrl Pts',(-21.1834934933002,21.3628760054068,21.5403751053906));
#50732=CARTESIAN_POINT('Ctrl Pts',(-21.1889370405964,21.3570110828813,21.5398707521407));
#50733=CARTESIAN_POINT('Ctrl Pts',(-21.1897246292117,21.3561634444223,21.5397978038088));
#50734=CARTESIAN_POINT('Ctrl Pts',(-21.1927233739582,21.3529395433453,21.5395201403116));
#50735=CARTESIAN_POINT('Ctrl Pts',(-21.1949376574447,21.3505662037471,21.5393152932233));
#50736=CARTESIAN_POINT('Ctrl Pts',(-21.2018592282405,21.343169877187,21.5386755283866));
#50737=CARTESIAN_POINT('Ctrl Pts',(-21.2065790035263,21.3381586494819,21.5382400844483));
#50738=CARTESIAN_POINT('Ctrl Pts',(-21.2150248724087,21.3292486086665,21.5374623019707));
#50739=CARTESIAN_POINT('Ctrl Pts',(-21.2187447761126,21.3253439421346,21.5371202250601));
#50740=CARTESIAN_POINT('Ctrl Pts',(-21.225243647245,21.3185564764754,21.5365234475031));
#50741=CARTESIAN_POINT('Ctrl Pts',(-21.2280182269136,21.3156694768229,21.5362689316827));
#50742=CARTESIAN_POINT('Ctrl Pts',(-21.2338451637871,21.3096290181086,21.5357349786288));
#50743=CARTESIAN_POINT('Ctrl Pts',(-21.2368985947419,21.3064766102146,21.5354554966424));
#50744=CARTESIAN_POINT('Ctrl Pts',(-21.2542941347665,21.2885904477104,21.5338650871084));
#50745=CARTESIAN_POINT('Ctrl Pts',(-21.2687702968871,21.2739882403019,21.532548564287));
#50746=CARTESIAN_POINT('Ctrl Pts',(-21.3015867580189,21.2415135798956,21.529579566751));
#50747=CARTESIAN_POINT('Ctrl Pts',(-21.3200022065971,21.2237193296554,21.5279240498435));
#50748=CARTESIAN_POINT('Ctrl Pts',(-21.4877190743648,21.0654812259741,21.5129415003928));
#50749=CARTESIAN_POINT('Ctrl Pts',(-21.6498750049879,20.9393755166254,21.4990790960961));
#50750=CARTESIAN_POINT('Ctrl Pts',(-21.9768945191604,20.7317522576256,21.4728685293787));
#50751=CARTESIAN_POINT('Ctrl Pts',(-22.1389528790534,20.6472112186308,21.4605802639441));
#50752=CARTESIAN_POINT('Ctrl Pts',(-22.3220088801862,20.5706906829568,21.4480303402257));
#50753=CARTESIAN_POINT('Ctrl Pts',(-22.3367507131747,20.5646563367365,21.4470287814219));
#50754=CARTESIAN_POINT('Ctrl Pts',(-22.3550227095693,20.5573346685479,21.4457991494938));
#50755=CARTESIAN_POINT('Ctrl Pts',(-22.3585108400397,20.5559440298942,21.4455649398828));
#50756=CARTESIAN_POINT('Ctrl Pts',(-22.3640020249789,20.5537659340301,21.4451970741876));
#50757=CARTESIAN_POINT('Ctrl Pts',(-22.3660034372074,20.5529743869543,21.4450631704608));
#50758=CARTESIAN_POINT('Ctrl Pts',(-22.3697419484449,20.5515001563102,21.4448133753987));
#50759=CARTESIAN_POINT('Ctrl Pts',(-22.3714788360296,20.5508169813828,21.4446974548023));
#50760=CARTESIAN_POINT('Ctrl Pts',(-22.3753745595173,20.549288571912,21.4444377488541));
#50761=CARTESIAN_POINT('Ctrl Pts',(-22.3775337098141,20.548444159676,21.4442940140166));
#50762=CARTESIAN_POINT('Ctrl Pts',(-22.3830147101582,20.5463074364644,21.4439296550492));
#50763=CARTESIAN_POINT('Ctrl Pts',(-22.3863378061927,20.5450183013521,21.4437092229923));
#50764=CARTESIAN_POINT('Ctrl Pts',(-22.4045323413241,20.5379947654678,21.4425048886088));
#50765=CARTESIAN_POINT('Ctrl Pts',(-22.4194443682585,20.5323651038765,21.4415272156349));
#50766=CARTESIAN_POINT('Ctrl Pts',(-22.7047422274933,20.4270696531969,21.4229897534602));
#50767=CARTESIAN_POINT('Ctrl Pts',(-22.9872980339362,20.3639845908132,21.4074088819883));
#50768=CARTESIAN_POINT('Ctrl Pts',(-23.4776899933444,20.3218728230987,21.3797236754214));
#50769=CARTESIAN_POINT('Ctrl Pts',(-23.6820262323926,20.3237501344491,21.3680127498266));
#50770=CARTESIAN_POINT('Ctrl Pts',(-23.8939507061801,20.3458690022281,21.3550717404019));
#50771=CARTESIAN_POINT('Ctrl Pts',(-23.9030987697753,20.3468634250469,21.354511645616));
#50772=CARTESIAN_POINT('Ctrl Pts',(-23.9195910549072,20.34872769017,21.3534991829551));
#50773=CARTESIAN_POINT('Ctrl Pts',(-23.9269368043547,20.3495836620799,21.3530472543973));
#50774=CARTESIAN_POINT('Ctrl Pts',(-23.9382381784198,20.3509400122082,21.3523504472496));
#50775=CARTESIAN_POINT('Ctrl Pts',(-23.9421959630792,20.3514224634079,21.3521061357713));
#50776=CARTESIAN_POINT('Ctrl Pts',(-23.9494711209888,20.3523230046028,21.3516565134875));
#50777=CARTESIAN_POINT('Ctrl Pts',(-23.9527887625422,20.3527389156166,21.3514512718982));
#50778=CARTESIAN_POINT('Ctrl Pts',(-23.9594512463146,20.3535846810685,21.3510386950811));
#50779=CARTESIAN_POINT('Ctrl Pts',(-23.9627960728795,20.3540146241285,21.3508313572882));
#50780=CARTESIAN_POINT('Ctrl Pts',(-23.9722947016508,20.3552507338016,21.3502419653532));
#50781=CARTESIAN_POINT('Ctrl Pts',(-23.9784468337084,20.3560694247609,21.3498595149603));
#50782=CARTESIAN_POINT('Ctrl Pts',(-24.0044133431682,20.3596012672809,21.3482422684021));
#50783=CARTESIAN_POINT('Ctrl Pts',(-24.0242042684565,20.3624810129112,21.347002202715));
#50784=CARTESIAN_POINT('Ctrl Pts',(-24.3790082545516,20.4174850463712,21.3246333413055));
#50785=CARTESIAN_POINT('Ctrl Pts',(-24.7036891996217,20.5219639699789,21.3016197148811));
#50786=CARTESIAN_POINT('Ctrl Pts',(-25.1468697287346,20.7463520463564,21.2681403038743));
#50787=CARTESIAN_POINT('Ctrl Pts',(-25.2823165760869,20.8279350089339,21.2576409852094));
#50788=CARTESIAN_POINT('Ctrl Pts',(-25.4159422793815,20.9224488219498,21.247389895776));
#50789=CARTESIAN_POINT('Ctrl Pts',(-25.4206240696381,20.9257790830124,21.2470308877893));
#50790=CARTESIAN_POINT('Ctrl Pts',(-25.4273756936981,20.9306089052621,21.2465134160943));
#50791=CARTESIAN_POINT('Ctrl Pts',(-25.4294526544687,20.9320984121835,21.2463542644137));
#50792=CARTESIAN_POINT('Ctrl Pts',(-25.4330674215601,20.9346972850043,21.2460773391012));
#50793=CARTESIAN_POINT('Ctrl Pts',(-25.434606022495,20.9358055385864,21.2459594880669));
#50794=CARTESIAN_POINT('Ctrl Pts',(-25.437586446444,20.9379563343926,21.2457312394325));
#50795=CARTESIAN_POINT('Ctrl Pts',(-25.4390283804383,20.9389987099754,21.2456208306434));
#50796=CARTESIAN_POINT('Ctrl Pts',(-25.4424741162307,20.9414939833386,21.2453570326675));
#50797=CARTESIAN_POINT('Ctrl Pts',(-25.4444771126155,20.9429479990909,21.245203721492));
#50798=CARTESIAN_POINT('Ctrl Pts',(-25.4516512214461,20.9481684608988,21.2446547222017));
#50799=CARTESIAN_POINT('Ctrl Pts',(-25.4568128359416,20.9519480274436,21.244259941028));
#50800=CARTESIAN_POINT('Ctrl Pts',(-25.5336176212561,21.0085400443383,21.2383882031243));
#50801=CARTESIAN_POINT('Ctrl Pts',(-25.6030619142668,21.0642886397747,21.2331128075798));
#50802=CARTESIAN_POINT('Ctrl Pts',(-25.8952026840257,21.3194163486235,21.2106332411874));
#50803=CARTESIAN_POINT('Ctrl Pts',(-26.0918650738679,21.546342504079,21.1945976724144));
#50804=CARTESIAN_POINT('Ctrl Pts',(-26.2992994144198,21.8663121079944,21.1725912511314));
#50805=CARTESIAN_POINT('Ctrl Pts',(-26.3414719885852,21.9371789314685,21.1677606118491));
#50806=CARTESIAN_POINT('Ctrl Pts',(-26.4012692396846,22.0470424871649,21.1602834321609));
#50807=CARTESIAN_POINT('Ctrl Pts',(-26.4209127537955,22.0849039961281,21.1577088655693));
#50808=CARTESIAN_POINT('Ctrl Pts',(-26.4431651964723,22.1299597163883,21.1546438123051));
#50809=CARTESIAN_POINT('Ctrl Pts',(-26.4465078023684,22.1367884278796,21.1541792366905));
#50810=CARTESIAN_POINT('Ctrl Pts',(-26.4515956676129,22.1472764072274,21.153465639436));
#50811=CARTESIAN_POINT('Ctrl Pts',(-26.4533582540513,22.1509272790293,21.1532172225354));
#50812=CARTESIAN_POINT('Ctrl Pts',(-26.4565616631364,22.1575946518619,21.1527635251345));
#50813=CARTESIAN_POINT('Ctrl Pts',(-26.4580046921053,22.1606100916206,21.1525583217946));
#50814=CARTESIAN_POINT('Ctrl Pts',(-26.4608979412386,22.1666802362267,21.1521452196053));
#50815=CARTESIAN_POINT('Ctrl Pts',(-26.4623480505527,22.1697349889617,21.1519373172263));
#50816=CARTESIAN_POINT('Ctrl Pts',(-26.4664654128397,22.178443843313,21.1513445669054));
#50817=CARTESIAN_POINT('Ctrl Pts',(-26.469121014194,22.1841034085512,21.150959315377));
#50818=CARTESIAN_POINT('Ctrl Pts',(-26.4803602394371,22.2082385931714,21.1493161914307));
#50819=CARTESIAN_POINT('Ctrl Pts',(-26.4887848911462,22.2267873330876,21.1480528384583));
#50820=CARTESIAN_POINT('Ctrl Pts',(-26.6420104939896,22.572824274073,21.1244701309282));
#50821=CARTESIAN_POINT('Ctrl Pts',(-26.7313776087769,22.9220523620919,21.1000146521633));
#50822=CARTESIAN_POINT('Ctrl Pts',(-26.7692016465279,23.3692710965809,21.0698813376803));
#50823=CARTESIAN_POINT('Ctrl Pts',(-26.773027258957,23.4601788548242,21.063840734755));
#50824=CARTESIAN_POINT('Ctrl Pts',(-26.7730018072047,23.5533447254896,21.05780963281));
#50825=CARTESIAN_POINT('Ctrl Pts',(-26.7729989260515,23.5555565090896,21.0576665454831));
#50826=CARTESIAN_POINT('Ctrl Pts',(-26.7728873014182,23.6034208899777,21.0545720766094));
#50827=CARTESIAN_POINT('Ctrl Pts',(-26.7718107820078,23.6490690752659,21.0516608112858));
#50828=CARTESIAN_POINT('Ctrl Pts',(-26.769541542956,23.6996533018269,21.0484902808158));
#50829=CARTESIAN_POINT('Ctrl Pts',(-26.7693070011791,23.7046243277756,21.0481793015351));
#50830=CARTESIAN_POINT('Ctrl Pts',(-26.7689392265204,23.7120535928113,21.0477154497589));
#50831=CARTESIAN_POINT('Ctrl Pts',(-26.7688146914049,23.7145122254959,21.0475620923194));
#50832=CARTESIAN_POINT('Ctrl Pts',(-26.7685954786253,23.7187440494801,21.0472983914782));
#50833=CARTESIAN_POINT('Ctrl Pts',(-26.768502152638,23.7205173047894,21.0471879717434));
#50834=CARTESIAN_POINT('Ctrl Pts',(-26.7683060238771,23.7241861040194,21.0469596810447));
#50835=CARTESIAN_POINT('Ctrl Pts',(-26.7682030120461,23.7260816309643,21.0468418226378));
#50836=CARTESIAN_POINT('Ctrl Pts',(-26.7679566700315,23.7305418513955,21.0465647101373));
#50837=CARTESIAN_POINT('Ctrl Pts',(-26.7678119478885,23.733106473519,21.0464055349741));
#50838=CARTESIAN_POINT('Ctrl Pts',(-26.7673295353918,23.7414773773002,21.0458865168385));
#50839=CARTESIAN_POINT('Ctrl Pts',(-26.7669791909521,23.7472829612408,21.0455273848965));
#50840=CARTESIAN_POINT('Ctrl Pts',(-26.7581535166614,23.8872318797028,21.0368895022321));
#50841=CARTESIAN_POINT('Ctrl Pts',(-26.7413087671498,24.0207354106358,21.0290757419086));
#50842=CARTESIAN_POINT('Ctrl Pts',(-26.6882718021546,24.2993972774105,21.0129497331154));
#50843=CARTESIAN_POINT('Ctrl Pts',(-26.6502254734612,24.4438706194493,21.0046923196446));
#50844=CARTESIAN_POINT('Ctrl Pts',(-26.5585486132173,24.7142272253037,20.9886819832602));
#50845=CARTESIAN_POINT('Ctrl Pts',(-26.5066568509048,24.8403499684541,20.9809639523108));
#50846=CARTESIAN_POINT('Ctrl Pts',(-26.4355590366025,24.9861489744099,20.9714849461523));
#50847=CARTESIAN_POINT('Ctrl Pts',(-26.4238927951812,25.0093562995406,20.9699589125314));
#50848=CARTESIAN_POINT('Ctrl Pts',(-26.4096615937357,25.0368332000321,20.9681302095878));
#50849=CARTESIAN_POINT('Ctrl Pts',(-26.4073654619362,25.0412414555393,20.9678361441981));
#50850=CARTESIAN_POINT('Ctrl Pts',(-26.4031901239435,25.0492124650575,20.967303174538));
#50851=CARTESIAN_POINT('Ctrl Pts',(-26.4013144161027,25.0527770466902,20.9670643835585));
#50852=CARTESIAN_POINT('Ctrl Pts',(-26.3974786620677,25.0600334417291,20.9665773520772));
#50853=CARTESIAN_POINT('Ctrl Pts',(-26.3955181069003,25.0637249761414,20.9663290953305));
#50854=CARTESIAN_POINT('Ctrl Pts',(-26.3687145288299,25.1139573503009,20.9629442192677));
#50855=CARTESIAN_POINT('Ctrl Pts',(-26.3427407212253,25.1598829254286,20.9597705125149));
#50856=CARTESIAN_POINT('Ctrl Pts',(-26.311173177963,25.2126336074033,20.9560241672819));
#50857=CARTESIAN_POINT('Ctrl Pts',(-26.306663465352,25.2201005542173,20.9554914670565));
#50858=CARTESIAN_POINT('Ctrl Pts',(-26.2998927574783,25.2312089745229,20.9546953591865));
#50859=CARTESIAN_POINT('Ctrl Pts',(-26.2976546968246,25.2348644385419,20.9544327951914));
#50860=CARTESIAN_POINT('Ctrl Pts',(-26.2936479786439,25.2413794605155,20.9539637809001));
#50861=CARTESIAN_POINT('Ctrl Pts',(-26.2918821226178,25.244240741147,20.9537574341554));
#50862=CARTESIAN_POINT('Ctrl Pts',(-26.2881477534328,25.2502705409727,20.9533218122562));
#50863=CARTESIAN_POINT('Ctrl Pts',(-26.2861782115737,25.2534384144091,20.9530924992705));
#50864=CARTESIAN_POINT('Ctrl Pts',(-26.2809568396855,25.2618042071213,20.9524857278489));
#50865=CARTESIAN_POINT('Ctrl Pts',(-26.2776956799303,25.2669962597002,20.952107923928));
#50866=CARTESIAN_POINT('Ctrl Pts',(-26.2628288426025,25.2905162838023,20.9503908749893));
#50867=CARTESIAN_POINT('Ctrl Pts',(-26.2510533221876,25.3087357481076,20.9490453184085));
#50868=CARTESIAN_POINT('Ctrl Pts',(-26.1630777561412,25.4418860498269,20.9390954298873));
#50869=CARTESIAN_POINT('Ctrl Pts',(-26.0797652834811,25.5519241303697,20.9302197366731));
#50870=CARTESIAN_POINT('Ctrl Pts',(-25.7855138590326,25.8927570860636,20.9005066776176));
#50871=CARTESIAN_POINT('Ctrl Pts',(-25.5480825583942,26.0982655623259,20.8787385536476));
#50872=CARTESIAN_POINT('Ctrl Pts',(-25.246700280964,26.2907319727763,20.855626032057));
#50873=CARTESIAN_POINT('Ctrl Pts',(-25.2080770796704,26.3142678758738,20.852742807674));
#50874=CARTESIAN_POINT('Ctrl Pts',(-25.1642634226804,26.3397177167375,20.8495702199671));
#50875=CARTESIAN_POINT('Ctrl Pts',(-25.1595509793027,26.342439073161,20.84923024015));
#50876=CARTESIAN_POINT('Ctrl Pts',(-25.1528489461287,26.3462867807029,20.848748522453));
#50877=CARTESIAN_POINT('Ctrl Pts',(-25.1508650492827,26.3474229515662,20.8486061507337));
#50878=CARTESIAN_POINT('Ctrl Pts',(-25.1472263888802,26.349501661112,20.8483454390283));
#50879=CARTESIAN_POINT('Ctrl Pts',(-25.1455719964545,26.350444845536,20.8482270568815));
#50880=CARTESIAN_POINT('Ctrl Pts',(-25.1422029046419,26.3523616410342,20.8479862957927));
#50881=CARTESIAN_POINT('Ctrl Pts',(-25.1404881475576,26.3533351449371,20.8478639239));
#50882=CARTESIAN_POINT('Ctrl Pts',(-25.1362120997725,26.3557575611737,20.8475591828491));
#50883=CARTESIAN_POINT('Ctrl Pts',(-25.1336497093308,26.3572045441147,20.8473769394166));
#50884=CARTESIAN_POINT('Ctrl Pts',(-25.1241508416554,26.3625514126747,20.8467027143346));
#50885=CARTESIAN_POINT('Ctrl Pts',(-25.1172018345671,26.3664291546104,20.8462121548542));
#50886=CARTESIAN_POINT('Ctrl Pts',(-24.9968316091776,26.4330156616264,20.8377596558871));
#50887=CARTESIAN_POINT('Ctrl Pts',(-24.8797276158142,26.4888609453313,20.8302230754313));
#50888=CARTESIAN_POINT('Ctrl Pts',(-24.494364114994,26.6448651712481,20.8065735411277));
#50889=CARTESIAN_POINT('Ctrl Pts',(-24.2160600643983,26.7164302572485,20.7910796570363));
#50890=CARTESIAN_POINT('Ctrl Pts',(-23.8414481126276,26.7611139310924,20.7690468673939));
#50891=CARTESIAN_POINT('Ctrl Pts',(-23.7505304943422,26.768064229153,20.7636233801982));
#50892=CARTESIAN_POINT('Ctrl Pts',(-23.6502912030961,26.7714625129638,20.7575176537741));
#50893=CARTESIAN_POINT('Ctrl Pts',(-23.6411346500995,26.7717338550978,20.756958775833));
#50894=CARTESIAN_POINT('Ctrl Pts',(-23.6274995895303,26.7720797331281,20.7561248126053));
#50895=CARTESIAN_POINT('Ctrl Pts',(-23.6230218268349,26.7721839793198,20.7558506599002));
#50896=CARTESIAN_POINT('Ctrl Pts',(-23.6153386226538,26.7723468260231,20.7553797695941));
#50897=CARTESIAN_POINT('Ctrl Pts',(-23.6121332752645,26.7724099788478,20.7551831751004));
#50898=CARTESIAN_POINT('Ctrl Pts',(-23.6058829070043,26.77252379566,20.7547995360351));
#50899=CARTESIAN_POINT('Ctrl Pts',(-23.6028378976609,26.7725749265559,20.7546125063621));
#50900=CARTESIAN_POINT('Ctrl Pts',(-23.5955316897556,26.7726872512719,20.7541634297809));
#50901=CARTESIAN_POINT('Ctrl Pts',(-23.5912704419927,26.7727443090068,20.7539012533242));
#50902=CARTESIAN_POINT('Ctrl Pts',(-23.5785803446872,26.7728890533702,20.7531197086612));
#50903=CARTESIAN_POINT('Ctrl Pts',(-23.5701512995601,26.7729521225188,20.7525995685115));
#50904=CARTESIAN_POINT('Ctrl Pts',(-23.5073406835446,26.7731756643591,20.7487159143166));
#50905=CARTESIAN_POINT('Ctrl Pts',(-23.4529659093277,26.771992694252,20.7453104418377));
#50906=CARTESIAN_POINT('Ctrl Pts',(-23.2670113586736,26.7632354247391,20.7335055310453));
#50907=CARTESIAN_POINT('Ctrl Pts',(-23.13589320398,26.7489684563823,20.7249026666826));
#50908=CARTESIAN_POINT('Ctrl Pts',(-22.7744937684843,26.6870499851088,20.7004848184321));
#50909=CARTESIAN_POINT('Ctrl Pts',(-22.548004468906,26.6221886440398,20.6843225063893));
#50910=CARTESIAN_POINT('Ctrl Pts',(-22.2470990819667,26.4991579554132,20.6628185173757));
#50911=CARTESIAN_POINT('Ctrl Pts',(-22.1650760488437,26.4615309056342,20.6569622107838));
#50912=CARTESIAN_POINT('Ctrl Pts',(-22.0814970208994,26.4188563737905,20.6510791518621));
#50913=CARTESIAN_POINT('Ctrl Pts',(-22.0782651224947,26.4171993084604,20.6508517966473));
#50914=CARTESIAN_POINT('Ctrl Pts',(-22.075036015346,26.4155367745563,20.6506247785903));
#50915=CARTESIAN_POINT('',(-26.7730010559745,23.5472555922587,20.8139447069714));
#50916=CARTESIAN_POINT('Ctrl Pts',(-22.0750362907684,26.4155369163599,20.4058188292237));
#50917=CARTESIAN_POINT('Ctrl Pts',(-22.1523064855167,26.4553201388708,20.4116349747003));
#50918=CARTESIAN_POINT('Ctrl Pts',(-22.2311828084613,26.4919760493018,20.4175106537931));
#50919=CARTESIAN_POINT('Ctrl Pts',(-22.5058363542375,26.6063346039196,20.437648250673));
#50920=CARTESIAN_POINT('Ctrl Pts',(-22.7076827246404,26.6680305312452,20.4519346842536));
#50921=CARTESIAN_POINT('Ctrl Pts',(-22.9264732946551,26.7120835996383,20.4660137596104));
#50922=CARTESIAN_POINT('Ctrl Pts',(-22.9388368567904,26.7144976428897,20.4668045901101));
#50923=CARTESIAN_POINT('Ctrl Pts',(-22.9547765093788,26.7175130216683,20.4678177616358));
#50924=CARTESIAN_POINT('Ctrl Pts',(-22.9583396781558,26.7181808576871,20.4680438359248));
#50925=CARTESIAN_POINT('Ctrl Pts',(-22.9637832674892,26.7191916314723,20.4683885823665));
#50926=CARTESIAN_POINT('Ctrl Pts',(-22.9656628636199,26.7195389081493,20.4685075028351));
#50927=CARTESIAN_POINT('Ctrl Pts',(-22.9691922350996,26.7201877529406,20.468730584559));
#50928=CARTESIAN_POINT('Ctrl Pts',(-22.9708419306316,26.7204897043026,20.468834767424));
#50929=CARTESIAN_POINT('Ctrl Pts',(-22.9746350755554,26.7211809213828,20.4690741088026));
#50930=CARTESIAN_POINT('Ctrl Pts',(-22.9767786805125,26.7215693008648,20.4692092157328));
#50931=CARTESIAN_POINT('Ctrl Pts',(-22.981177103669,26.7223616040677,20.4694861322266));
#50932=CARTESIAN_POINT('Ctrl Pts',(-22.9834319627591,26.7227652980241,20.4696279285624));
#50933=CARTESIAN_POINT('Ctrl Pts',(-22.9943115308698,26.7247011293229,20.4703112986211));
#50934=CARTESIAN_POINT('Ctrl Pts',(-23.0029421421396,26.7262005219933,20.4708510145859));
#50935=CARTESIAN_POINT('Ctrl Pts',(-23.1114218682976,26.7445913277403,20.4776059942336));
#50936=CARTESIAN_POINT('Ctrl Pts',(-23.2120190386022,26.7568044977116,20.4835642969508));
#50937=CARTESIAN_POINT('Ctrl Pts',(-23.4775917041439,26.7764057110331,20.4988830161048));
#50938=CARTESIAN_POINT('Ctrl Pts',(-23.642846677961,26.7758960733521,20.5080116531318));
#50939=CARTESIAN_POINT('Ctrl Pts',(-24.038989460624,26.7441932777891,20.5302612977874));
#50940=CARTESIAN_POINT('Ctrl Pts',(-24.2679119404094,26.7006593014154,20.5434666341156));
#50941=CARTESIAN_POINT('Ctrl Pts',(-24.5044768630513,26.6285309283383,20.5584720689336));
#50942=CARTESIAN_POINT('Ctrl Pts',(-24.5187747733948,26.6240623204228,20.559384166739));
#50943=CARTESIAN_POINT('Ctrl Pts',(-24.5382971150868,26.6178111578869,20.5606368090709));
#50944=CARTESIAN_POINT('Ctrl Pts',(-24.5435490478157,26.6161145726807,20.560974519208));
#50945=CARTESIAN_POINT('Ctrl Pts',(-24.5518721152959,26.613402256363,20.5615108651133));
#50946=CARTESIAN_POINT('Ctrl Pts',(-24.5549461401831,26.6123953727339,20.5617092084694));
#50947=CARTESIAN_POINT('Ctrl Pts',(-24.5609012922427,26.6104348556145,20.5620939367427));
#50948=CARTESIAN_POINT('Ctrl Pts',(-24.5637825997442,26.6094817767644,20.5622803031566));
#50949=CARTESIAN_POINT('Ctrl Pts',(-24.5706358335474,26.6072041195578,20.5627241082573));
#50950=CARTESIAN_POINT('Ctrl Pts',(-24.5746065257973,26.6058758703509,20.5629816682379));
#50951=CARTESIAN_POINT('Ctrl Pts',(-24.5828242414452,26.6031091174612,20.563515595594));
#50952=CARTESIAN_POINT('Ctrl Pts',(-24.587070871416,26.6016694811014,20.5637920001121));
#50953=CARTESIAN_POINT('Ctrl Pts',(-24.6112042972258,26.5934318906887,20.5653655957975));
#50954=CARTESIAN_POINT('Ctrl Pts',(-24.6310268506934,26.586448522978,20.566668934191));
#50955=CARTESIAN_POINT('Ctrl Pts',(-24.682777722786,26.5676459952776,20.5701006378737));
#50956=CARTESIAN_POINT('Ctrl Pts',(-24.7145888631145,26.5555141486923,20.5722393412261));
#50957=CARTESIAN_POINT('Ctrl Pts',(-24.856988589716,26.4986067439709,20.5819483954631));
#50958=CARTESIAN_POINT('Ctrl Pts',(-24.9652199125761,26.4482196433584,20.5897040854235));
#50959=CARTESIAN_POINT('Ctrl Pts',(-25.1612393851782,26.3433605112384,20.604441217498));
#50960=CARTESIAN_POINT('Ctrl Pts',(-25.249692367879,26.2904410367293,20.6113746009179));
#50961=CARTESIAN_POINT('Ctrl Pts',(-25.5259268831231,26.1066500617984,20.6338118853973));
#50962=CARTESIAN_POINT('Ctrl Pts',(-25.7023821753626,25.9599863460388,20.6494234485337));
#50963=CARTESIAN_POINT('Ctrl Pts',(-25.8713237679461,25.7860815953571,20.6647326967004));
#50964=CARTESIAN_POINT('Ctrl Pts',(-25.8807578478583,25.776246303639,20.6655887769634));
#50965=CARTESIAN_POINT('Ctrl Pts',(-25.8926679872287,25.7636709341808,20.6666706997264));
#50966=CARTESIAN_POINT('Ctrl Pts',(-25.8952019304493,25.7609862353312,20.6669009515372));
#50967=CARTESIAN_POINT('Ctrl Pts',(-25.899211145194,25.7567238457955,20.6672653548127));
#50968=CARTESIAN_POINT('Ctrl Pts',(-25.9006894434654,25.7551490262573,20.6673997406585));
#50969=CARTESIAN_POINT('Ctrl Pts',(-25.9033141903275,25.7523472646403,20.6676383810484));
#50970=CARTESIAN_POINT('Ctrl Pts',(-25.9044612566809,25.7511209197223,20.66774268363));
#50971=CARTESIAN_POINT('Ctrl Pts',(-25.9071257028015,25.7482678561199,20.6679849896626));
#50972=CARTESIAN_POINT('Ctrl Pts',(-25.9086423546224,25.7466404651604,20.668122936356));
#50973=CARTESIAN_POINT('Ctrl Pts',(-25.91176124163,25.7432868958118,20.6684066618127));
#50974=CARTESIAN_POINT('Ctrl Pts',(-25.9133632726611,25.7415605281462,20.6685524248168));
#50975=CARTESIAN_POINT('Ctrl Pts',(-25.9174593716336,25.7371368074287,20.6689251857035));
#50976=CARTESIAN_POINT('Ctrl Pts',(-25.919950730959,25.7344369339888,20.6691519772616));
#50977=CARTESIAN_POINT('Ctrl Pts',(-25.9533030182125,25.6981689945561,20.6721890899786));
#50978=CARTESIAN_POINT('Ctrl Pts',(-25.9834546994167,25.6639517788309,20.674946405766));
#50979=CARTESIAN_POINT('Ctrl Pts',(-26.0900465954939,25.5376824124136,20.6847866983229));
#50980=CARTESIAN_POINT('Ctrl Pts',(-26.1620782633659,25.4420250354175,20.6916186736561));
#50981=CARTESIAN_POINT('Ctrl Pts',(-26.2542866093905,25.3042325015594,20.7009601914171));
#50982=CARTESIAN_POINT('Ctrl Pts',(-26.2791186285383,25.2653431866167,20.7035448255219));
#50983=CARTESIAN_POINT('Ctrl Pts',(-26.32806496526,25.1849328068545,20.7088096288835));
#50984=CARTESIAN_POINT('Ctrl Pts',(-26.3521033959923,25.1433794116713,20.7114887703956));
#50985=CARTESIAN_POINT('Ctrl Pts',(-26.4926565797461,24.8873879938935,20.7278213538405));
#50986=CARTESIAN_POINT('Ctrl Pts',(-26.5854126861312,24.6608607622563,20.7416314138394));
#50987=CARTESIAN_POINT('Ctrl Pts',(-26.6558067190603,24.4115754219983,20.7573471200967));
#50988=CARTESIAN_POINT('Ctrl Pts',(-26.6597939469514,24.397067804836,20.7582631894038));
#50989=CARTESIAN_POINT('Ctrl Pts',(-26.6651073179554,24.3771913415142,20.7595204413289));
#50990=CARTESIAN_POINT('Ctrl Pts',(-26.6665214895856,24.3718460541619,20.7598587623665));
#50991=CARTESIAN_POINT('Ctrl Pts',(-26.6687416724536,24.3633660033418,20.7603958410737));
#50992=CARTESIAN_POINT('Ctrl Pts',(-26.6695567335596,24.3602336024056,20.7605943048999));
#50993=CARTESIAN_POINT('Ctrl Pts',(-26.6711267140367,24.3541624189672,20.7609791129234));
#50994=CARTESIAN_POINT('Ctrl Pts',(-26.6718822050751,24.3512237865074,20.7611654383721));
#50995=CARTESIAN_POINT('Ctrl Pts',(-26.6736691436834,24.3442322044633,20.761608904425));
#50996=CARTESIAN_POINT('Ctrl Pts',(-26.6746968523132,24.3401783129604,20.7618661657917));
#50997=CARTESIAN_POINT('Ctrl Pts',(-26.6768084680937,24.3317802571916,20.7623993805358));
#50998=CARTESIAN_POINT('Ctrl Pts',(-26.6778912184387,24.3274358138165,20.7626753707722));
#50999=CARTESIAN_POINT('Ctrl Pts',(-26.6806859772603,24.3161216545832,20.7633945245292));
#51000=CARTESIAN_POINT('Ctrl Pts',(-26.6823837565231,24.3091484795207,20.7638381472929));
#51001=CARTESIAN_POINT('Ctrl Pts',(-26.7433977334457,24.0548572535618,20.7800303986883));
#51002=CARTESIAN_POINT('Ctrl Pts',(-26.7732375911853,23.8014572351736,20.7967802754889));
#51003=CARTESIAN_POINT('Ctrl Pts',(-26.7730011374811,23.547254799421,20.8139446178767));
#51004=CARTESIAN_POINT('Ctrl Pts',(-26.7730011382095,23.5472555825959,20.8139445649949));
#51005=CARTESIAN_POINT('Ctrl Pts',(-26.7727921327512,23.3225030001619,20.8291203840233));
#51006=CARTESIAN_POINT('Ctrl Pts',(-26.7490729694072,23.098366539446,20.8445032138022));
#51007=CARTESIAN_POINT('Ctrl Pts',(-26.6958354141065,22.8485668667248,20.8608633304296));
#51008=CARTESIAN_POINT('Ctrl Pts',(-26.6890289325242,22.8187217283387,20.8628040760745));
#51009=CARTESIAN_POINT('Ctrl Pts',(-26.6808645071488,22.7851369604993,20.8649687743573));
#51010=CARTESIAN_POINT('Ctrl Pts',(-26.6799239803867,22.7812988258202,20.8652158755795));
#51011=CARTESIAN_POINT('Ctrl Pts',(-26.6783836822329,22.7750627632368,20.8656168825299));
#51012=CARTESIAN_POINT('Ctrl Pts',(-26.677788211022,22.7726637928861,20.8657710329596));
#51013=CARTESIAN_POINT('Ctrl Pts',(-26.6766313305607,22.7680259044466,20.866068825276));
#51014=CARTESIAN_POINT('Ctrl Pts',(-26.6760702750183,22.7657869008487,20.8662124874847));
#51015=CARTESIAN_POINT('Ctrl Pts',(-26.675095017184,22.761912599239,20.8664608987368));
#51016=CARTESIAN_POINT('Ctrl Pts',(-26.6746819371511,22.7602770266377,20.866565713036));
#51017=CARTESIAN_POINT('Ctrl Pts',(-26.6738175161176,22.7568656729399,20.8667842119649));
#51018=CARTESIAN_POINT('Ctrl Pts',(-26.6733659462046,22.7550899573075,20.866897882724));
#51019=CARTESIAN_POINT('Ctrl Pts',(-26.6721135711785,22.7501827471399,20.8672118366497));
#51020=CARTESIAN_POINT('Ctrl Pts',(-26.6713095661025,22.7470520597101,20.8674119332869));
#51021=CARTESIAN_POINT('Ctrl Pts',(-26.668141971071,22.7347944436667,20.8681946141552));
#51022=CARTESIAN_POINT('Ctrl Pts',(-26.6657430147599,22.725676577237,20.8687751628499));
#51023=CARTESIAN_POINT('Ctrl Pts',(-26.6241969350058,22.5705396240489,20.8786268739988));
#51024=CARTESIAN_POINT('Ctrl Pts',(-26.5748570347339,22.4274201563866,20.8873245034422));
#51025=CARTESIAN_POINT('Ctrl Pts',(-26.4785941222552,22.2012217046486,20.9012044275201));
#51026=CARTESIAN_POINT('Ctrl Pts',(-26.437730163035,22.1158389861431,20.9064762155067));
#51027=CARTESIAN_POINT('Ctrl Pts',(-26.3729040947183,21.9944225721862,20.9141700201257));
#51028=CARTESIAN_POINT('Ctrl Pts',(-26.3518820032506,21.9568784520925,20.9165775372235));
#51029=CARTESIAN_POINT('Ctrl Pts',(-26.3091304509788,21.883990097554,20.9213244954035));
#51030=CARTESIAN_POINT('Ctrl Pts',(-26.2874577979167,21.8486224010182,20.9236628076672));
#51031=CARTESIAN_POINT('Ctrl Pts',(-26.2017602772345,21.7146476270852,20.9326818725866));
#51032=CARTESIAN_POINT('Ctrl Pts',(-26.1330455956362,21.6191609344149,20.939456392972));
#51033=CARTESIAN_POINT('Ctrl Pts',(-26.0242522802773,21.4842039971169,20.9497337895205));
#51034=CARTESIAN_POINT('Ctrl Pts',(-25.9881108910112,21.4416801848879,20.953083329168));
#51035=CARTESIAN_POINT('Ctrl Pts',(-25.9459926343167,21.3946550029867,20.9569250267958));
#51036=CARTESIAN_POINT('Ctrl Pts',(-25.9410812066175,21.3892088970462,20.9573720887902));
#51037=CARTESIAN_POINT('Ctrl Pts',(-25.9330971512043,21.3804161963649,20.9580973752472));
#51038=CARTESIAN_POINT('Ctrl Pts',(-25.9300359417327,21.3770592306239,20.9583751162673));
#51039=CARTESIAN_POINT('Ctrl Pts',(-25.924111034239,21.3705894240193,20.9589120199538));
#51040=CARTESIAN_POINT('Ctrl Pts',(-25.9212482847561,21.3674757241033,20.9591711419717));
#51041=CARTESIAN_POINT('Ctrl Pts',(-25.9163169114261,21.362133211301,20.9596170042816));
#51042=CARTESIAN_POINT('Ctrl Pts',(-25.9142512425142,21.3599016683733,20.9598036180266));
#51043=CARTESIAN_POINT('Ctrl Pts',(-25.9099931098655,21.3553146461409,20.9601879929204));
#51044=CARTESIAN_POINT('Ctrl Pts',(-25.9078002707893,21.3529595208566,20.9603857700791));
#51045=CARTESIAN_POINT('Ctrl Pts',(-25.9018950916233,21.3466363310161,20.9609179262825));
#51046=CARTESIAN_POINT('Ctrl Pts',(-25.8981762491165,21.3426743776647,20.961252585113));
#51047=CARTESIAN_POINT('Ctrl Pts',(-25.884545626096,21.3282260874537,20.9624775037632));
#51048=CARTESIAN_POINT('Ctrl Pts',(-25.8745735838389,21.3177970662608,20.9633703702267));
#51049=CARTESIAN_POINT('Ctrl Pts',(-25.7040340205788,21.1418236369081,20.978586120084));
#51050=CARTESIAN_POINT('Ctrl Pts',(-25.5262578946383,20.9939531096286,20.9937178731558));
#51051=CARTESIAN_POINT('Ctrl Pts',(-25.2617521789707,20.8181345998484,21.0151120521346));
#51052=CARTESIAN_POINT('Ctrl Pts',(-25.187313697625,20.7728923044465,21.0210163202554));
#51053=CARTESIAN_POINT('Ctrl Pts',(-25.0303236950414,20.6859831761106,21.0331509988955));
#51054=CARTESIAN_POINT('Ctrl Pts',(-24.9476218454735,20.644738790083,21.0393741091326));
#51055=CARTESIAN_POINT('Ctrl Pts',(-24.8022532128371,20.5798865100468,21.0499124629924));
#51056=CARTESIAN_POINT('Ctrl Pts',(-24.7404110827491,20.5545716480462,21.0542761233911));
#51057=CARTESIAN_POINT('Ctrl Pts',(-24.6600439154961,20.5245557835005,21.0597568338974));
#51058=CARTESIAN_POINT('Ctrl Pts',(-24.6422066007105,20.5180727747416,21.0609614422618));
#51059=CARTESIAN_POINT('Ctrl Pts',(-24.6133983214508,20.5078895360428,21.0628867985817));
#51060=CARTESIAN_POINT('Ctrl Pts',(-24.6024631629157,20.5040902962169,21.0636129898798));
#51061=CARTESIAN_POINT('Ctrl Pts',(-24.5891467335978,20.4995439872799,21.0644914800653));
#51062=CARTESIAN_POINT('Ctrl Pts',(-24.5867849486927,20.4987407204238,21.0646470653156));
#51063=CARTESIAN_POINT('Ctrl Pts',(-24.5822204951197,20.4971942143576,21.0649473206063));
#51064=CARTESIAN_POINT('Ctrl Pts',(-24.5800179513921,20.4964506148909,21.0650920119377));
#51065=CARTESIAN_POINT('Ctrl Pts',(-24.5760450698021,20.4951141196346,21.0653526484068));
#51066=CARTESIAN_POINT('Ctrl Pts',(-24.5742750256108,20.4945203804592,21.0654686436767));
#51067=CARTESIAN_POINT('Ctrl Pts',(-24.5704675102114,20.4932468769059,21.0657178870387));
#51068=CARTESIAN_POINT('Ctrl Pts',(-24.5684298807565,20.4925676130474,21.065851104851));
#51069=CARTESIAN_POINT('Ctrl Pts',(-24.5629373876685,20.490742735431,21.0662097509332));
#51070=CARTESIAN_POINT('Ctrl Pts',(-24.5594812467131,20.489600932436,21.0664349524636));
#51071=CARTESIAN_POINT('Ctrl Pts',(-24.5435500831238,20.4843676835179,21.0674708652545));
#51072=CARTESIAN_POINT('Ctrl Pts',(-24.5310518349036,20.4803465610326,21.0682774615541));
#51073=CARTESIAN_POINT('Ctrl Pts',(-24.3011750431544,20.4079343535329,21.0830073033051));
#51074=CARTESIAN_POINT('Ctrl Pts',(-24.077132272913,20.3627014815647,21.0956590075224));
#51075=CARTESIAN_POINT('Ctrl Pts',(-23.6933945807891,20.3268353959293,21.1171940481115));
#51076=CARTESIAN_POINT('Ctrl Pts',(-23.5357730024209,20.3236918946058,21.1259991396484));
#51077=CARTESIAN_POINT('Ctrl Pts',(-23.2775269301755,20.3374693997469,21.1409600060509));
#51078=CARTESIAN_POINT('Ctrl Pts',(-23.176810728117,20.3476141174725,21.1469264847005));
#51079=CARTESIAN_POINT('Ctrl Pts',(-23.0565669544134,20.3654749477016,21.1542793837881));
#51080=CARTESIAN_POINT('Ctrl Pts',(-23.0364179664536,20.3686636647107,21.1555192090957));
#51081=CARTESIAN_POINT('Ctrl Pts',(-23.0119189485747,20.3727795955675,21.1570365092037));
#51082=CARTESIAN_POINT('Ctrl Pts',(-23.0075384791076,20.3735248500468,21.157308187671));
#51083=CARTESIAN_POINT('Ctrl Pts',(-22.9990622995055,20.374984956148,21.1578346300345));
#51084=CARTESIAN_POINT('Ctrl Pts',(-22.9949664018427,20.3756986792431,21.1580893575627));
#51085=CARTESIAN_POINT('Ctrl Pts',(-22.9878869511581,20.3769464161276,21.158530223052));
#51086=CARTESIAN_POINT('Ctrl Pts',(-22.9849027421508,20.3774767178956,21.1587162424331));
#51087=CARTESIAN_POINT('Ctrl Pts',(-22.9787231375743,20.3785838451094,21.1591018219234));
#51088=CARTESIAN_POINT('Ctrl Pts',(-22.9755278578233,20.3791612912977,21.1593014016571));
#51089=CARTESIAN_POINT('Ctrl Pts',(-22.9677786809363,20.3805738080612,21.1597859303523));
#51090=CARTESIAN_POINT('Ctrl Pts',(-22.9632257093455,20.3814138631338,21.160071038233));
#51091=CARTESIAN_POINT('Ctrl Pts',(-22.9462243019876,20.3845886400384,21.1611372746563));
#51092=CARTESIAN_POINT('Ctrl Pts',(-22.9337879809414,20.3869869046054,21.1619204313958));
#51093=CARTESIAN_POINT('Ctrl Pts',(-22.7251617949627,20.4284961387105,21.175113338792));
#51094=CARTESIAN_POINT('Ctrl Pts',(-22.533056844298,20.4857095673268,21.1881221420755));
#51095=CARTESIAN_POINT('Ctrl Pts',(-22.2374529887695,20.6046200509834,21.2094483280828));
#51096=CARTESIAN_POINT('Ctrl Pts',(-22.129915157384,20.6549402092976,21.2174958706886));
#51097=CARTESIAN_POINT('Ctrl Pts',(-21.9261477253604,20.7643785578314,21.2331388246394));
#51098=CARTESIAN_POINT('Ctrl Pts',(-21.8297522837839,20.8228559415908,21.2407254515604));
#51099=CARTESIAN_POINT('Ctrl Pts',(-21.6947137898143,20.9147900048912,21.2514523838317));
#51100=CARTESIAN_POINT('Ctrl Pts',(-21.6534909437703,20.9443011012999,21.2547407511839));
#51101=CARTESIAN_POINT('Ctrl Pts',(-21.5992484807865,20.9851022524049,21.2590685511161));
#51102=CARTESIAN_POINT('Ctrl Pts',(-21.5856003573141,20.9955402924251,21.2601575485867));
#51103=CARTESIAN_POINT('Ctrl Pts',(-21.5635678890573,21.0126716449259,21.2619147634004));
#51104=CARTESIAN_POINT('Ctrl Pts',(-21.5551325360386,21.0192983960233,21.2625873428073));
#51105=CARTESIAN_POINT('Ctrl Pts',(-21.5448206954604,21.0274828917107,21.2634091442458));
#51106=CARTESIAN_POINT('Ctrl Pts',(-21.5429128174517,21.0290007041448,21.2635611756874));
#51107=CARTESIAN_POINT('Ctrl Pts',(-21.5392209425244,21.0319446223573,21.2638553313842));
#51108=CARTESIAN_POINT('Ctrl Pts',(-21.5374367364749,21.0333704618583,21.2639974745525));
#51109=CARTESIAN_POINT('Ctrl Pts',(-21.5341987584375,21.0359637212908,21.2642554043354));
#51110=CARTESIAN_POINT('Ctrl Pts',(-21.5327444888813,21.037130502023,21.2643712362386));
#51111=CARTESIAN_POINT('Ctrl Pts',(-21.5298154179576,21.0394847174763,21.2646045114512));
#51112=CARTESIAN_POINT('Ctrl Pts',(-21.5283406564428,21.0406721850546,21.264721951451));
#51113=CARTESIAN_POINT('Ctrl Pts',(-21.5241149268194,21.0440808555849,21.2650584281871));
#51114=CARTESIAN_POINT('Ctrl Pts',(-21.5213665554737,21.0463052958682,21.265277230641));
#51115=CARTESIAN_POINT('Ctrl Pts',(-21.5094538822647,21.055979507756,21.2662254785313));
#51116=CARTESIAN_POINT('Ctrl Pts',(-21.5003267579419,21.0634752240618,21.2669516365414));
#51117=CARTESIAN_POINT('Ctrl Pts',(-21.3429697090199,21.1941608836205,21.2794688742194));
#51118=CARTESIAN_POINT('Ctrl Pts',(-21.2060186076234,21.3303749077204,21.290341154348));
#51119=CARTESIAN_POINT('Ctrl Pts',(-20.9830677574113,21.5959300012872,21.3097517552693));
#51120=CARTESIAN_POINT('Ctrl Pts',(-20.8926622071128,21.720764605568,21.3182942230691));
#51121=CARTESIAN_POINT('Ctrl Pts',(-20.7539003391431,21.9444863795487,21.3333094040662));
#51122=CARTESIAN_POINT('Ctrl Pts',(-20.7010439386487,22.0402599832638,21.3396520222094));
#51123=CARTESIAN_POINT('Ctrl Pts',(-20.6316748945658,22.1826167835442,21.3490880874659));
#51124=CARTESIAN_POINT('Ctrl Pts',(-20.6112009948454,22.2271884265678,21.352043084181));
#51125=CARTESIAN_POINT('Ctrl Pts',(-20.5886419645478,22.2794095243182,21.3555118811041));
#51126=CARTESIAN_POINT('Ctrl Pts',(-20.5855573468342,22.2866222218401,21.3559911276612));
#51127=CARTESIAN_POINT('Ctrl Pts',(-20.5808811351877,22.2976678853251,21.3567252970675));
#51128=CARTESIAN_POINT('Ctrl Pts',(-20.5792705450404,22.3014928184456,21.356979572175));
#51129=CARTESIAN_POINT('Ctrl Pts',(-20.5764968737343,22.3081156510503,21.3574199274378));
#51130=CARTESIAN_POINT('Ctrl Pts',(-20.5753303389889,22.3109121060032,21.3576058898303));
#51131=CARTESIAN_POINT('Ctrl Pts',(-20.57292065159,22.3167116922946,21.3579916116321));
#51132=CARTESIAN_POINT('Ctrl Pts',(-20.5716780952815,22.3197150664502,21.358191391055));
#51133=CARTESIAN_POINT('Ctrl Pts',(-20.5686721361914,22.327011978183,21.3586768435755));
#51134=CARTESIAN_POINT('Ctrl Pts',(-20.5669134651032,22.331307446794,21.358962676875));
#51135=CARTESIAN_POINT('Ctrl Pts',(-20.5603617259512,22.3474088650356,21.3600343573398));
#51136=CARTESIAN_POINT('Ctrl Pts',(-20.5556294573177,22.3592392859217,21.3608222594028));
#51137=CARTESIAN_POINT('Ctrl Pts',(-20.4802408410799,22.5509968637151,21.37360207209));
#51138=CARTESIAN_POINT('Ctrl Pts',(-20.4258562455587,22.7368602445359,21.3861513337721));
#51139=CARTESIAN_POINT('Ctrl Pts',(-20.3442029508427,23.1507244204699,21.4143419722727));
#51140=CARTESIAN_POINT('Ctrl Pts',(-20.3239437527184,23.3790652436216,21.4300617275792));
#51141=CARTESIAN_POINT('Ctrl Pts',(-20.3290578705046,23.6662949112184,21.4490063443225));
#51142=CARTESIAN_POINT('Ctrl Pts',(-20.3317047874976,23.7249300410336,21.4528265863884));
#51143=CARTESIAN_POINT('Ctrl Pts',(-20.3379328850167,23.8107705269663,21.4583199875463));
#51144=CARTESIAN_POINT('Ctrl Pts',(-20.3402620674178,23.8380519064616,21.460051075185));
#51145=CARTESIAN_POINT('Ctrl Pts',(-20.3433680176967,23.8696716290291,21.4620376861545));
#51146=CARTESIAN_POINT('Ctrl Pts',(-20.3438062345163,23.8740410270414,21.4623117690602));
#51147=CARTESIAN_POINT('Ctrl Pts',(-20.3444884906843,23.8807064725274,21.4627291945464));
#51148=CARTESIAN_POINT('Ctrl Pts',(-20.3447260667965,23.8830031538801,21.4628729010207));
#51149=CARTESIAN_POINT('Ctrl Pts',(-20.345141498621,23.8869774552983,21.4631213617196));
#51150=CARTESIAN_POINT('Ctrl Pts',(-20.3453182030785,23.8886551880261,21.4632261812815));
#51151=CARTESIAN_POINT('Ctrl Pts',(-20.345689535868,23.8921544534432,21.4634446644937));
#51152=CARTESIAN_POINT('Ctrl Pts',(-20.3458843993825,23.8939759539105,21.4635583143144));
#51153=CARTESIAN_POINT('Ctrl Pts',(-20.3464271993913,23.8990092365172,21.4638721426703));
#51154=CARTESIAN_POINT('Ctrl Pts',(-20.3467784135314,23.9022206744904,21.4640721349297));
#51155=CARTESIAN_POINT('Ctrl Pts',(-20.3481722795643,23.9147910029119,21.4648540197704));
#51156=CARTESIAN_POINT('Ctrl Pts',(-20.349251133385,23.9241459540982,21.4654338819899));
#51157=CARTESIAN_POINT('Ctrl Pts',(-20.3678383229033,24.0793391451392,21.4750218515815));
#51158=CARTESIAN_POINT('Ctrl Pts',(-20.3952587229793,24.2238394442988,21.4834886618475));
#51159=CARTESIAN_POINT('Ctrl Pts',(-20.4779894461166,24.5400448355368,21.5019653230839));
#51160=CARTESIAN_POINT('Ctrl Pts',(-20.5380265742129,24.7099877412166,21.511873670238));
#51161=CARTESIAN_POINT('Ctrl Pts',(-20.6641771469372,24.9899966658131,21.5292730739882));
#51162=CARTESIAN_POINT('Ctrl Pts',(-20.7232348438092,25.1027538509832,21.5366013667223));
#51163=CARTESIAN_POINT('Ctrl Pts',(-20.8164992027969,25.2577647350456,21.5473562742163));
#51164=CARTESIAN_POINT('Ctrl Pts',(-20.8453487016055,25.3031073269847,21.5505896710549));
#51165=CARTESIAN_POINT('Ctrl Pts',(-20.8797457091292,25.3542963018213,21.5543498233421));
#51166=CARTESIAN_POINT('Ctrl Pts',(-20.8841987414649,25.3608706028859,21.5548348674714));
#51167=CARTESIAN_POINT('Ctrl Pts',(-20.8910538229761,25.3709110866383,21.5555789236728));
#51168=CARTESIAN_POINT('Ctrl Pts',(-20.8934384767695,25.3743891558063,21.5558372740943));
#51169=CARTESIAN_POINT('Ctrl Pts',(-20.8975533697025,25.3803656304476,21.5562822539938));
#51170=CARTESIAN_POINT('Ctrl Pts',(-20.8992803330538,25.3828662935632,21.5564687583272));
#51171=CARTESIAN_POINT('Ctrl Pts',(-20.9028459573322,25.3880137726772,21.5568533226747));
#51172=CARTESIAN_POINT('Ctrl Pts',(-20.9046850561564,25.3906602802879,21.5570513993143));
#51173=CARTESIAN_POINT('Ctrl Pts',(-20.9091250170645,25.3970290839555,21.5575289353297));
#51174=CARTESIAN_POINT('Ctrl Pts',(-20.9117297775595,25.4007486430388,21.5578085440082));
#51175=CARTESIAN_POINT('Ctrl Pts',(-20.9197574111078,25.4121605754442,21.5586686144669));
#51176=CARTESIAN_POINT('Ctrl Pts',(-20.9252060905819,25.4198346566076,21.5592500682428));
#51177=CARTESIAN_POINT('Ctrl Pts',(-20.9357194584114,25.4345054273612,21.560367638263));
#51178=CARTESIAN_POINT('Ctrl Pts',(-20.940778819584,25.4415058488317,21.5609035446771));
#51179=CARTESIAN_POINT('Ctrl Pts',(-20.9585635744139,25.4659066287333,21.5627808116796));
#51180=CARTESIAN_POINT('Ctrl Pts',(-20.9714351430267,25.4831992744263,21.5641278470677));
#51181=CARTESIAN_POINT('Ctrl Pts',(-20.9870922822228,25.5037994980044,21.5657528767401));
#51182=CARTESIAN_POINT('Ctrl Pts',(-20.9897124830592,25.5072325707068,21.5660243768376));
#51183=CARTESIAN_POINT('Ctrl Pts',(-20.9933219173451,25.5119421105574,21.5663977694145));
#51184=CARTESIAN_POINT('Ctrl Pts',(-20.9943052300207,25.5132231278746,21.5664994302704));
#51185=CARTESIAN_POINT('Ctrl Pts',(-20.9980084283727,25.5180399947065,21.5668820569986));
#51186=CARTESIAN_POINT('Ctrl Pts',(-21.0007346821009,25.5215709222163,21.5671632715307));
#51187=CARTESIAN_POINT('Ctrl Pts',(-21.0047315642741,25.52672535396,21.5675748669832));
#51188=CARTESIAN_POINT('Ctrl Pts',(-21.0059964419694,25.5283533285691,21.5677050231817));
#51189=CARTESIAN_POINT('Ctrl Pts',(-21.0115175117565,25.5354452252886,21.5682727084125));
#51190=CARTESIAN_POINT('Ctrl Pts',(-21.0157897247628,25.5408966011455,21.5687108618133));
#51191=CARTESIAN_POINT('Ctrl Pts',(-21.0231841420782,25.5502695424442,21.5694673047606));
#51192=CARTESIAN_POINT('Ctrl Pts',(-21.0262979966671,25.5541976890649,21.5697852684233));
#51193=CARTESIAN_POINT('Ctrl Pts',(-21.0319193827821,25.5612552155092,21.5703582416768));
#51194=CARTESIAN_POINT('Ctrl Pts',(-21.0344236196825,25.5643872164846,21.5706131230165));
#51195=CARTESIAN_POINT('Ctrl Pts',(-21.0396774737558,25.5709330248627,21.5711470910116));
#51196=CARTESIAN_POINT('Ctrl Pts',(-21.0424282216541,25.5743459106381,21.5714262211045));
#51197=CARTESIAN_POINT('Ctrl Pts',(-21.0580547138129,25.593653132208,21.5730094337762));
#51198=CARTESIAN_POINT('Ctrl Pts',(-21.0710743638938,25.609429930542,21.5743190527707));
#51199=CARTESIAN_POINT('Ctrl Pts',(-21.1187575411656,25.6661031168661,21.5790815586127));
#51200=CARTESIAN_POINT('Ctrl Pts',(-21.1542885819883,25.7062552767034,21.5825670414861));
#51201=CARTESIAN_POINT('Ctrl Pts',(-21.3519508353203,25.9187023583864,21.6016165662394));
#51202=CARTESIAN_POINT('Ctrl Pts',(-21.5316726594639,26.0736231944658,21.6178177105776));
#51203=CARTESIAN_POINT('Ctrl Pts',(-21.8007811381698,26.2583036758534,21.6397169868783));
#51204=CARTESIAN_POINT('Ctrl Pts',(-21.8769664172572,26.3060295951644,21.6456797894781));
#51205=CARTESIAN_POINT('Ctrl Pts',(-21.9945809519448,26.3730300788114,21.6544338920038));
#51206=CARTESIAN_POINT('Ctrl Pts',(-22.034584504871,26.3947099625176,21.657336253066));
#51207=CARTESIAN_POINT('Ctrl Pts',(-22.075036015355,26.4155367745608,21.6601868380444));
#51208=CARTESIAN_POINT('Origin',(-23.5502525316942,23.5502525316942,-77.3107734492734));
#51209=CARTESIAN_POINT('',(-22.0750359362463,26.4155367338311,23.156397107556));
#51210=CARTESIAN_POINT('',(-22.0750361284943,26.4155368328116,22.9065074728514));
#51211=CARTESIAN_POINT('',(-22.0750360153461,26.4155367745563,-77.3107734492734));
#51212=CARTESIAN_POINT('',(-26.7730014957921,23.5528365025921,22.3125994347384));
#51213=CARTESIAN_POINT('Ctrl Pts',(-22.0750359362473,26.4155367338316,23.1563971075561));
#51214=CARTESIAN_POINT('Ctrl Pts',(-22.0294856266012,26.3920847590964,23.1533709924801));
#51215=CARTESIAN_POINT('Ctrl Pts',(-21.9844639750547,26.3675308704831,23.1503081910084));
#51216=CARTESIAN_POINT('Ctrl Pts',(-21.9225276784368,26.3318054693836,23.1459836548566));
#51217=CARTESIAN_POINT('Ctrl Pts',(-21.9051394521694,26.3215568942344,23.1447571047244));
#51218=CARTESIAN_POINT('Ctrl Pts',(-21.8825127524228,26.3079327868681,23.1431442266346));
#51219=CARTESIAN_POINT('Ctrl Pts',(-21.8771859189913,26.3047042865337,23.1427632888179));
#51220=CARTESIAN_POINT('Ctrl Pts',(-21.8689857199637,26.29970172628,23.1421749550518));
#51221=CARTESIAN_POINT('Ctrl Pts',(-21.8661057064932,26.2979385466644,23.1419679595713));
#51222=CARTESIAN_POINT('Ctrl Pts',(-21.8603798731074,26.294420736762,23.141555696188));
#51223=CARTESIAN_POINT('Ctrl Pts',(-21.8575340016088,26.2926661981049,23.1413504318406));
#51224=CARTESIAN_POINT('Ctrl Pts',(-21.8513069420466,26.2888137013258,23.1409005007039));
#51225=CARTESIAN_POINT('Ctrl Pts',(-21.847926902625,26.2867139052174,23.1406557661818));
#51226=CARTESIAN_POINT('Ctrl Pts',(-21.8383055833703,26.2807120878993,23.1399576589943));
#51227=CARTESIAN_POINT('Ctrl Pts',(-21.8320738009395,26.2767949556607,23.1395037266934));
#51228=CARTESIAN_POINT('Ctrl Pts',(-21.8181259413803,26.2679608956485,23.1384837523374));
#51229=CARTESIAN_POINT('Ctrl Pts',(-21.8104172973801,26.2630324031619,23.1379172815519));
#51230=CARTESIAN_POINT('Ctrl Pts',(-21.7170415781639,26.2027712809842,23.1310217507204));
#51231=CARTESIAN_POINT('Ctrl Pts',(-21.6340353818574,26.1434409488034,23.1245424034599));
#51232=CARTESIAN_POINT('Ctrl Pts',(-21.3901394501606,25.9510001068978,23.104378714728));
#51233=CARTESIAN_POINT('Ctrl Pts',(-21.2392551950895,25.8061222650276,23.0902632779117));
#51234=CARTESIAN_POINT('Ctrl Pts',(-20.9819764320549,25.5059912143173,23.0635158983552));
#51235=CARTESIAN_POINT('Ctrl Pts',(-20.8730238244339,25.35397655252,23.0509478955615));
#51236=CARTESIAN_POINT('Ctrl Pts',(-20.7720180192221,25.1835500448935,23.0384642857336));
#51237=CARTESIAN_POINT('Ctrl Pts',(-20.7662522234357,25.1737025819987,23.0377483911955));
#51238=CARTESIAN_POINT('Ctrl Pts',(-20.7587922121724,25.1608049261938,23.0368180249622));
#51239=CARTESIAN_POINT('Ctrl Pts',(-20.7570505668576,25.1577824738107,23.036600520672));
#51240=CARTESIAN_POINT('Ctrl Pts',(-20.7543759510902,25.153123473828,23.0362660512508));
#51241=CARTESIAN_POINT('Ctrl Pts',(-20.7534395093714,25.1514889381363,23.0361488603861));
#51242=CARTESIAN_POINT('Ctrl Pts',(-20.7515787066757,25.1482343409376,23.035915820993));
#51243=CARTESIAN_POINT('Ctrl Pts',(-20.7506543243926,25.1466143074897,23.0357999717045));
#51244=CARTESIAN_POINT('Ctrl Pts',(-20.748593382147,25.1429950911444,23.0355414945063));
#51245=CARTESIAN_POINT('Ctrl Pts',(-20.7474575579343,25.1409954983833,23.0353989149486));
#51246=CARTESIAN_POINT('Ctrl Pts',(-20.7441364176982,25.1351341065389,23.0349816330491));
#51247=CARTESIAN_POINT('Ctrl Pts',(-20.7419569245714,25.131268987992,23.0347073079793));
#51248=CARTESIAN_POINT('Ctrl Pts',(-20.725978249816,25.1027950757905,23.0326924581769));
#51249=CARTESIAN_POINT('Ctrl Pts',(-20.7124942154485,25.0780095282868,23.030971931129));
#51250=CARTESIAN_POINT('Ctrl Pts',(-20.66923713237,24.9959476580317,23.0253736443429));
#51251=CARTESIAN_POINT('Ctrl Pts',(-20.6408575420404,24.9379506648075,23.0215721522811));
#51252=CARTESIAN_POINT('Ctrl Pts',(-20.5511588992428,24.7397718903957,23.0089683042789));
#51253=CARTESIAN_POINT('Ctrl Pts',(-20.498079092189,24.5960835294767,23.0004573386922));
#51254=CARTESIAN_POINT('Ctrl Pts',(-20.4376789161569,24.3881318169421,22.988356280251));
#51255=CARTESIAN_POINT('Ctrl Pts',(-20.4217623318041,24.3265933669076,22.9848021771545));
#51256=CARTESIAN_POINT('Ctrl Pts',(-20.3635218342693,24.0703892983238,22.9700046316717));
#51257=CARTESIAN_POINT('Ctrl Pts',(-20.3374769326493,23.8725096185598,22.9585392420737));
#51258=CARTESIAN_POINT('Ctrl Pts',(-20.3293919729415,23.6612698640343,22.9456905723071));
#51259=CARTESIAN_POINT('Ctrl Pts',(-20.3289933059839,23.6490279400181,22.9449439449603));
#51260=CARTESIAN_POINT('Ctrl Pts',(-20.3285418857962,23.6322214874948,22.9439160776453));
#51261=CARTESIAN_POINT('Ctrl Pts',(-20.3284290261296,23.6276585666661,22.9436367251243));
#51262=CARTESIAN_POINT('Ctrl Pts',(-20.3282528759963,23.6198672411692,22.9431592243023));
#51263=CARTESIAN_POINT('Ctrl Pts',(-20.3281847432504,23.616638943348,22.9429612282145));
#51264=CARTESIAN_POINT('Ctrl Pts',(-20.3280619534226,23.6103745784463,22.9425767405232));
#51265=CARTESIAN_POINT('Ctrl Pts',(-20.3280067352895,23.6073385252698,22.9423902667769));
#51266=CARTESIAN_POINT('Ctrl Pts',(-20.327886781405,23.6001872227056,22.9419507269586));
#51267=CARTESIAN_POINT('Ctrl Pts',(-20.3278256380497,23.5960719257129,22.9416975483793));
#51268=CARTESIAN_POINT('Ctrl Pts',(-20.327669144174,23.5839796004908,22.9409528995672));
#51269=CARTESIAN_POINT('Ctrl Pts',(-20.3275955302543,23.5760023652272,22.9404607477067));
#51270=CARTESIAN_POINT('Ctrl Pts',(-20.3274958047619,23.5579190291457,22.9393430059669));
#51271=CARTESIAN_POINT('Ctrl Pts',(-20.3274876099435,23.5478129501646,22.9387168573638));
#51272=CARTESIAN_POINT('Ctrl Pts',(-20.3276132790061,23.5155305511483,22.9367118864099));
#51273=CARTESIAN_POINT('Ctrl Pts',(-20.3279285087689,23.4933559545997,22.9353273963986));
#51274=CARTESIAN_POINT('Ctrl Pts',(-20.3300367739292,23.4074480943806,22.9299345675532));
#51275=CARTESIAN_POINT('Ctrl Pts',(-20.3334920137916,23.3437737624049,22.9258749650053));
#51276=CARTESIAN_POINT('Ctrl Pts',(-20.3534447864056,23.1064572425327,22.9105047436555));
#51277=CARTESIAN_POINT('Ctrl Pts',(-20.3821376953363,22.9341612346731,22.8988430960653));
#51278=CARTESIAN_POINT('Ctrl Pts',(-20.4625867824517,22.6139189454461,22.8765199912576));
#51279=CARTESIAN_POINT('Ctrl Pts',(-20.5114663647476,22.4657329612724,22.8659182803312));
#51280=CARTESIAN_POINT('Ctrl Pts',(-20.6035473576453,22.2424335707768,22.849971039027));
#51281=CARTESIAN_POINT('Ctrl Pts',(-20.6393685890608,22.1645326518966,22.8444161986524));
#51282=CARTESIAN_POINT('Ctrl Pts',(-20.6811345435415,22.0824924127031,22.8386454412202));
#51283=CARTESIAN_POINT('Ctrl Pts',(-20.6840289919902,22.0768481680136,22.8382488373415));
#51284=CARTESIAN_POINT('Ctrl Pts',(-20.6880718719515,22.0690214508559,22.837699494469));
#51285=CARTESIAN_POINT('Ctrl Pts',(-20.6892061480703,22.0668317435498,22.8375458701627));
#51286=CARTESIAN_POINT('Ctrl Pts',(-20.6911620184713,22.0630665457324,22.8372818319936));
#51287=CARTESIAN_POINT('Ctrl Pts',(-20.691982402123,22.0614904331442,22.8371713413541));
#51288=CARTESIAN_POINT('Ctrl Pts',(-20.6936816357499,22.058232464826,22.8369430224617));
#51289=CARTESIAN_POINT('Ctrl Pts',(-20.6945606661568,22.0565507098397,22.8368252065961));
#51290=CARTESIAN_POINT('Ctrl Pts',(-20.6966311506284,22.0525979811106,22.8365483932295));
#51291=CARTESIAN_POINT('Ctrl Pts',(-20.6978238341719,22.0503276452347,22.8363894741691));
#51292=CARTESIAN_POINT('Ctrl Pts',(-20.7017195509733,22.0429333946192,22.8358721268964));
#51293=CARTESIAN_POINT('Ctrl Pts',(-20.7044337103009,22.0378153064557,22.8355144033565));
#51294=CARTESIAN_POINT('Ctrl Pts',(-20.7992985395595,21.8600882588314,22.8231042435046));
#51295=CARTESIAN_POINT('Ctrl Pts',(-20.9069815288534,21.6961899708524,22.8120389351957));
#51296=CARTESIAN_POINT('Ctrl Pts',(-21.1583310962629,21.3804545465824,22.789432643089));
#51297=CARTESIAN_POINT('Ctrl Pts',(-21.3031888274897,21.2307675540355,22.7779389305399));
#51298=CARTESIAN_POINT('Ctrl Pts',(-21.4872982626294,21.074068017082,22.7639063103323));
#51299=CARTESIAN_POINT('Ctrl Pts',(-21.5134960899819,21.0524748890101,22.7619226849152));
#51300=CARTESIAN_POINT('Ctrl Pts',(-21.5512996152547,21.0223061899788,22.7590751815641));
#51301=CARTESIAN_POINT('Ctrl Pts',(-21.5626298037318,21.0133880593897,22.7582236136345));
#51302=CARTESIAN_POINT('Ctrl Pts',(-21.577273874756,21.0020198584459,22.7571251399503));
#51303=CARTESIAN_POINT('Ctrl Pts',(-21.5805332464755,20.9994996085439,22.75688078633));
#51304=CARTESIAN_POINT('Ctrl Pts',(-21.5864756701902,20.9949229192107,22.7564355271128));
#51305=CARTESIAN_POINT('Ctrl Pts',(-21.5891571453894,20.9928644352364,22.7562346963609));
#51306=CARTESIAN_POINT('Ctrl Pts',(-21.6006062268373,20.9841039318333,22.7553775814658));
#51307=CARTESIAN_POINT('Ctrl Pts',(-21.6094049152077,20.9774428077131,22.7547198096132));
#51308=CARTESIAN_POINT('Ctrl Pts',(-21.6190793868246,20.9701965336061,22.7539975010224));
#51309=CARTESIAN_POINT('Ctrl Pts',(-21.6199215166211,20.9695664134344,22.7539346342481));
#51310=CARTESIAN_POINT('Ctrl Pts',(-21.6261806360865,20.9648878307536,22.7534674346821));
#51311=CARTESIAN_POINT('Ctrl Pts',(-21.6316100183117,20.9608560380786,22.7530624860344));
#51312=CARTESIAN_POINT('Ctrl Pts',(-21.6428613353737,20.952555763129,22.7522239330439));
#51313=CARTESIAN_POINT('Ctrl Pts',(-21.6486849982771,20.9482896972556,22.7517902418336));
#51314=CARTESIAN_POINT('Ctrl Pts',(-21.6780768720993,20.9269103527649,22.7496030462664));
#51315=CARTESIAN_POINT('Ctrl Pts',(-21.7018613904171,20.9100979924343,22.7478383699771));
#51316=CARTESIAN_POINT('Ctrl Pts',(-21.7311779365365,20.8899655844337,22.7456683788759));
#51317=CARTESIAN_POINT('Ctrl Pts',(-21.7364968265927,20.8863363795274,22.7452748825211));
#51318=CARTESIAN_POINT('Ctrl Pts',(-21.7452847580442,20.880378685516,22.7446250642391));
#51319=CARTESIAN_POINT('Ctrl Pts',(-21.7487475317798,20.8780409469868,22.7443690933184));
#51320=CARTESIAN_POINT('Ctrl Pts',(-21.7549959487003,20.873840270088,22.7439073483533));
#51321=CARTESIAN_POINT('Ctrl Pts',(-21.7577799748001,20.8719749274296,22.7437016655747));
#51322=CARTESIAN_POINT('Ctrl Pts',(-21.7631828130233,20.8683671356644,22.7433026022862));
#51323=CARTESIAN_POINT('Ctrl Pts',(-21.7658012776569,20.8666241709331,22.7431092415386));
#51324=CARTESIAN_POINT('Ctrl Pts',(-21.7731144436023,20.8617716431597,22.7425693193893));
#51325=CARTESIAN_POINT('Ctrl Pts',(-21.7778147327559,20.8586705581305,22.7422224395463));
#51326=CARTESIAN_POINT('Ctrl Pts',(-21.7970272382894,20.8460669730783,22.7408050985251));
#51327=CARTESIAN_POINT('Ctrl Pts',(-21.8116077253638,20.8366695343733,22.7397307115008));
#51328=CARTESIAN_POINT('Ctrl Pts',(-21.8487311888421,20.81316468755,22.7369979965829));
#51329=CARTESIAN_POINT('Ctrl Pts',(-21.8713738883013,20.7992179664644,22.7353337989818));
#51330=CARTESIAN_POINT('Ctrl Pts',(-21.9629085596965,20.744388311402,22.7286149681981));
#51331=CARTESIAN_POINT('Ctrl Pts',(-22.0331367067531,20.7058030794041,22.7234788606682));
#51332=CARTESIAN_POINT('Ctrl Pts',(-22.2092703441057,20.6174097294622,22.7106405432937));
#51333=CARTESIAN_POINT('Ctrl Pts',(-22.3165863799123,20.5706780978902,22.7028524618182));
#51334=CARTESIAN_POINT('Ctrl Pts',(-22.6744805295177,20.4374846590288,22.6771428471074));
#51335=CARTESIAN_POINT('Ctrl Pts',(-22.9332226815881,20.3760450274932,22.6588843291175));
#51336=CARTESIAN_POINT('Ctrl Pts',(-23.2111126328635,20.3453632170192,22.6412152730107));
#51337=CARTESIAN_POINT('Ctrl Pts',(-23.2256582477367,20.3438573657034,22.64029619405));
#51338=CARTESIAN_POINT('Ctrl Pts',(-23.2439868840392,20.3420858770928,22.6391457747624));
#51339=CARTESIAN_POINT('Ctrl Pts',(-23.2477604976396,20.3417278706833,22.638909329542));
#51340=CARTESIAN_POINT('Ctrl Pts',(-23.2537082232285,20.3411741904085,22.6385373157019));
#51341=CARTESIAN_POINT('Ctrl Pts',(-23.2558819020991,20.3409740676322,22.6384014960658));
#51342=CARTESIAN_POINT('Ctrl Pts',(-23.2598945234828,20.3406087510652,22.6381510291662));
#51343=CARTESIAN_POINT('Ctrl Pts',(-23.2617333937795,20.3404429300896,22.6380363470437));
#51344=CARTESIAN_POINT('Ctrl Pts',(-23.2658348342985,20.3400766338268,22.6377807804083));
#51345=CARTESIAN_POINT('Ctrl Pts',(-23.268097469101,20.3398769707092,22.6376399426855));
#51346=CARTESIAN_POINT('Ctrl Pts',(-23.2746474358085,20.3393059558921,22.6372326700662));
#51347=CARTESIAN_POINT('Ctrl Pts',(-23.2789353240046,20.3389407973937,22.6369665853078));
#51348=CARTESIAN_POINT('Ctrl Pts',(-23.3082474081903,20.3365036951715,22.6351511909765));
#51349=CARTESIAN_POINT('Ctrl Pts',(-23.3332952477626,20.3347156100164,22.6336176552514));
#51350=CARTESIAN_POINT('Ctrl Pts',(-23.4106018212385,20.3301044119027,22.6289323112359));
#51351=CARTESIAN_POINT('Ctrl Pts',(-23.4629126925399,20.328261119802,22.6258289724947));
#51352=CARTESIAN_POINT('Ctrl Pts',(-23.5977787730171,20.3267961732674,22.6179480650913));
#51353=CARTESIAN_POINT('Ctrl Pts',(-23.6803181577387,20.3290704273155,22.6132402428225));
#51354=CARTESIAN_POINT('Ctrl Pts',(-23.7867936240093,20.3361041671926,22.6072175979802));
#51355=CARTESIAN_POINT('Ctrl Pts',(-23.8108852856798,20.3379679887335,22.6058582751057));
#51356=CARTESIAN_POINT('Ctrl Pts',(-23.8553834212792,20.3419144337549,22.603350501961));
#51357=CARTESIAN_POINT('Ctrl Pts',(-23.8757952732173,20.3439212728061,22.6022013039689));
#51358=CARTESIAN_POINT('Ctrl Pts',(-23.9138389495851,20.3480286615516,22.6000595834871));
#51359=CARTESIAN_POINT('Ctrl Pts',(-23.9314752204364,20.3500803391235,22.5990667898238));
#51360=CARTESIAN_POINT('Ctrl Pts',(-24.0991207347398,20.3709885484075,22.5896238125828));
#51361=CARTESIAN_POINT('Ctrl Pts',(-24.2476409683955,20.4002331201207,22.5812033823822));
#51362=CARTESIAN_POINT('Ctrl Pts',(-24.4478027244104,20.4545005170167,22.5693095686106));
#51363=CARTESIAN_POINT('Ctrl Pts',(-24.5016559021833,20.4706246238554,22.5660549323881));
#51364=CARTESIAN_POINT('Ctrl Pts',(-24.5728059222371,20.4939719440984,22.5616648961709));
#51365=CARTESIAN_POINT('Ctrl Pts',(-24.5905025752557,20.4999498755925,22.5605654877765));
#51366=CARTESIAN_POINT('Ctrl Pts',(-24.6122975806048,20.5075239546534,22.559201690625));
#51367=CARTESIAN_POINT('Ctrl Pts',(-24.6164461753879,20.508975169575,22.5589416577133));
#51368=CARTESIAN_POINT('Ctrl Pts',(-24.6243753502341,20.511767082749,22.5584438088016));
#51369=CARTESIAN_POINT('Ctrl Pts',(-24.6281564234462,20.5131063625575,22.5582060361354));
#51370=CARTESIAN_POINT('Ctrl Pts',(-24.6365806748776,20.5161079981572,22.5576754428675));
#51371=CARTESIAN_POINT('Ctrl Pts',(-24.6412225510467,20.5177739577295,22.5573825126318));
#51372=CARTESIAN_POINT('Ctrl Pts',(-24.6523847688375,20.5218090004708,22.5566767305347));
#51373=CARTESIAN_POINT('Ctrl Pts',(-24.6589013016606,20.5241884884644,22.5562635581188));
#51374=CARTESIAN_POINT('Ctrl Pts',(-24.6672333612256,20.5272614358488,22.5557337979316));
#51375=CARTESIAN_POINT('Ctrl Pts',(-24.6690560467098,20.5279355341134,22.5556178192519));
#51376=CARTESIAN_POINT('Ctrl Pts',(-24.6762503746342,20.5306036695003,22.5551596800309));
#51377=CARTESIAN_POINT('Ctrl Pts',(-24.6816172821205,20.5326103736302,22.5548171205081));
#51378=CARTESIAN_POINT('Ctrl Pts',(-24.6900645748282,20.5357945465981,22.5542766829216));
#51379=CARTESIAN_POINT('Ctrl Pts',(-24.6931485696979,20.536962455419,22.554079110519));
#51380=CARTESIAN_POINT('Ctrl Pts',(-24.7049882715268,20.5414669413087,22.5533195862047));
#51381=CARTESIAN_POINT('Ctrl Pts',(-24.7137311424152,20.5448369402369,22.5527565633212));
#51382=CARTESIAN_POINT('Ctrl Pts',(-24.7474573256393,20.5580061457724,22.550576152204));
#51383=CARTESIAN_POINT('Ctrl Pts',(-24.7723320215965,20.5680789274423,22.548949875087));
#51384=CARTESIAN_POINT('Ctrl Pts',(-24.8033797758997,20.5811051148179,22.5468961950661));
#51385=CARTESIAN_POINT('Ctrl Pts',(-24.8096736299409,20.5837692990651,22.5464786459062));
#51386=CARTESIAN_POINT('Ctrl Pts',(-24.8199136360275,20.5881423489507,22.5457972638406));
#51387=CARTESIAN_POINT('Ctrl Pts',(-24.8238649488127,20.589839137378,22.5455338434655));
#51388=CARTESIAN_POINT('Ctrl Pts',(-24.8309012179966,20.5928773743596,22.5450638713835));
#51389=CARTESIAN_POINT('Ctrl Pts',(-24.8339874981815,20.5942157567827,22.5448574248266));
#51390=CARTESIAN_POINT('Ctrl Pts',(-24.8399474511042,20.5968114173135,22.5444581607208));
#51391=CARTESIAN_POINT('Ctrl Pts',(-24.8428213961254,20.5980680639046,22.5442653650037));
#51392=CARTESIAN_POINT('Ctrl Pts',(-24.8490362541187,20.6007963560008,22.5438478676805));
#51393=CARTESIAN_POINT('Ctrl Pts',(-24.8523765074184,20.6022694853319,22.543623115311));
#51394=CARTESIAN_POINT('Ctrl Pts',(-24.8655058465643,20.6080864969675,22.5427382588186));
#51395=CARTESIAN_POINT('Ctrl Pts',(-24.8752756717864,20.6124734501513,22.542076674785));
#51396=CARTESIAN_POINT('Ctrl Pts',(-24.8982429138315,20.6229243243866,22.5405138986608));
#51397=CARTESIAN_POINT('Ctrl Pts',(-24.911421479434,20.6290288859931,22.539611310803));
#51398=CARTESIAN_POINT('Ctrl Pts',(-24.9572124967345,20.6506172903928,22.5364543537283));
#51399=CARTESIAN_POINT('Ctrl Pts',(-24.9896047195518,20.666559416184,22.53418416907));
#51400=CARTESIAN_POINT('Ctrl Pts',(-25.0647688774001,20.7051340867787,22.5288274286654));
#51401=CARTESIAN_POINT('Ctrl Pts',(-25.1073115477299,20.728192016466,22.5257266239043));
#51402=CARTESIAN_POINT('Ctrl Pts',(-25.2238916655606,20.7948165780329,22.517035417073));
#51403=CARTESIAN_POINT('Ctrl Pts',(-25.2967272135852,20.8403965296302,22.51138127237));
#51404=CARTESIAN_POINT('Ctrl Pts',(-25.6035816771314,21.0499372675898,22.4866215705518));
#51405=CARTESIAN_POINT('Ctrl Pts',(-25.8170309507082,21.2416926638815,22.4668000165846));
#51406=CARTESIAN_POINT('Ctrl Pts',(-26.0278170006795,21.48886333833,22.4458862001614));
#51407=CARTESIAN_POINT('Ctrl Pts',(-26.0526837845216,21.5191224830323,22.4433959550025));
#51408=CARTESIAN_POINT('Ctrl Pts',(-26.0799531982397,21.5535665711086,22.4406459273989));
#51409=CARTESIAN_POINT('Ctrl Pts',(-26.0829039415134,21.5573107050079,22.4403480962656));
#51410=CARTESIAN_POINT('Ctrl Pts',(-26.0873332816242,21.5629567223269,22.4399006513088));
#51411=CARTESIAN_POINT('Ctrl Pts',(-26.0888180549757,21.5648537179306,22.4397505984412));
#51412=CARTESIAN_POINT('Ctrl Pts',(-26.0913850854771,21.5681410285696,22.4394910641656));
#51413=CARTESIAN_POINT('Ctrl Pts',(-26.0924683292816,21.5695305660347,22.4393815118633));
#51414=CARTESIAN_POINT('Ctrl Pts',(-26.0947221767741,21.5724265970931,22.4391535042866));
#51415=CARTESIAN_POINT('Ctrl Pts',(-26.0958925809651,21.5739332402133,22.4390350637315));
#51416=CARTESIAN_POINT('Ctrl Pts',(-26.0986691865047,21.5775140801665,22.4387539887334));
#51417=CARTESIAN_POINT('Ctrl Pts',(-26.1002741990882,21.5795892066713,22.4385914397221));
#51418=CARTESIAN_POINT('Ctrl Pts',(-26.1056171148346,21.5865145384822,22.4380500754735));
#51419=CARTESIAN_POINT('Ctrl Pts',(-26.1093437576189,21.5913734752935,22.4376720592038));
#51420=CARTESIAN_POINT('Ctrl Pts',(-26.2047948356282,21.716563455267,22.427978210685));
#51421=CARTESIAN_POINT('Ctrl Pts',(-26.287960429666,21.8432142291866,22.4192509232727));
#51422=CARTESIAN_POINT('Ctrl Pts',(-26.4579711859301,22.1467169014364,22.3995842960208));
#51423=CARTESIAN_POINT('Ctrl Pts',(-26.5381304636759,22.3265993257044,22.3887853651874));
#51424=CARTESIAN_POINT('Ctrl Pts',(-26.6076789564656,22.5311151579963,22.376489520812));
#51425=CARTESIAN_POINT('Ctrl Pts',(-26.6137855886801,22.5496214695126,22.3753770230729));
#51426=CARTESIAN_POINT('Ctrl Pts',(-26.63363539814,22.6116622401787,22.3716458693469));
#51427=CARTESIAN_POINT('Ctrl Pts',(-26.6466209849791,22.6554319910262,22.3690108293393));
#51428=CARTESIAN_POINT('Ctrl Pts',(-26.6840184469967,22.7920660319612,22.3607551023492));
#51429=CARTESIAN_POINT('Ctrl Pts',(-26.7052117208723,22.8857487288143,22.35505031585));
#51430=CARTESIAN_POINT('Ctrl Pts',(-26.7239911231415,22.990248510911,22.3485874383871));
#51431=CARTESIAN_POINT('Ctrl Pts',(-26.7257438333153,23.0002742232777,22.3479664124362));
#51432=CARTESIAN_POINT('Ctrl Pts',(-26.7281490532456,23.0144272622646,22.3470882958149));
#51433=CARTESIAN_POINT('Ctrl Pts',(-26.7288410849276,23.018547886206,22.3468324634961));
#51434=CARTESIAN_POINT('Ctrl Pts',(-26.7300372423039,23.0257560647712,22.346384635088));
#51435=CARTESIAN_POINT('Ctrl Pts',(-26.7305448905388,23.0288430363726,22.3461927512635));
#51436=CARTESIAN_POINT('Ctrl Pts',(-26.7315590723543,23.035066785749,22.3458056902112));
#51437=CARTESIAN_POINT('Ctrl Pts',(-26.7320654633471,23.0382035825448,22.3456105087088));
#51438=CARTESIAN_POINT('Ctrl Pts',(-26.7330959784469,23.0446475789257,22.3452093331585));
#51439=CARTESIAN_POINT('Ctrl Pts',(-26.7336195886335,23.0479548555506,22.3450033230348));
#51440=CARTESIAN_POINT('Ctrl Pts',(-26.7348240557317,23.0556401566997,22.344524340208));
#51441=CARTESIAN_POINT('Ctrl Pts',(-26.7355010393109,23.0600187735546,22.34425124472));
#51442=CARTESIAN_POINT('Ctrl Pts',(-26.7372342476121,23.0713840384052,22.3435418642406));
#51443=CARTESIAN_POINT('Ctrl Pts',(-26.7382765235008,23.0783727611506,22.3431051369837));
#51444=CARTESIAN_POINT('Ctrl Pts',(-26.7618657746906,23.2401906352954,22.332980949314));
#51445=CARTESIAN_POINT('Ctrl Pts',(-26.773126904686,23.3964255372188,22.3229329672665));
#51446=CARTESIAN_POINT('Ctrl Pts',(-26.7730014957921,23.5528365025921,22.3125994347384));
#51447=CARTESIAN_POINT('Ctrl Pts',(-26.7730014989634,23.5528325442904,22.3125996962497));
#51448=CARTESIAN_POINT('Ctrl Pts',(-26.7727816966704,23.8273922941403,22.2944604890385));
#51449=CARTESIAN_POINT('Ctrl Pts',(-26.7374794702398,24.1007806232849,22.2754700028552));
#51450=CARTESIAN_POINT('Ctrl Pts',(-26.6498300776261,24.4356096374394,22.2526975769606));
#51451=CARTESIAN_POINT('Ctrl Pts',(-26.6294062724549,24.5042191084543,22.2480663482769));
#51452=CARTESIAN_POINT('Ctrl Pts',(-26.6031299350747,24.5828147945174,22.2428459527465));
#51453=CARTESIAN_POINT('Ctrl Pts',(-26.5994904084202,24.5935135953152,22.242137184495));
#51454=CARTESIAN_POINT('Ctrl Pts',(-26.5947045595185,24.6073431252165,22.2412236243568));
#51455=CARTESIAN_POINT('Ctrl Pts',(-26.5936096103835,24.6104913559544,22.2410158321948));
#51456=CARTESIAN_POINT('Ctrl Pts',(-26.5918307224937,24.615580606502,22.2406802181609));
#51457=CARTESIAN_POINT('Ctrl Pts',(-26.5911498089548,24.6175226694417,22.2405522161276));
#51458=CARTESIAN_POINT('Ctrl Pts',(-26.5898419267614,24.6212415241408,22.2403072384408));
#51459=CARTESIAN_POINT('Ctrl Pts',(-26.5892152621287,24.6230184127659,22.2401902453797));
#51460=CARTESIAN_POINT('Ctrl Pts',(-26.5877746976747,24.6270916977328,22.2399221868232));
#51461=CARTESIAN_POINT('Ctrl Pts',(-26.5869597499704,24.6293877266076,22.2397711843011));
#51462=CARTESIAN_POINT('Ctrl Pts',(-26.5843808965873,24.6366273187334,22.2392953579153));
#51463=CARTESIAN_POINT('Ctrl Pts',(-26.582607505501,24.641567530361,22.2389710991441));
#51464=CARTESIAN_POINT('Ctrl Pts',(-26.5679018994689,24.6822209622872,22.2363061969817));
#51465=CARTESIAN_POINT('Ctrl Pts',(-26.5543506365233,24.7177092208651,22.2340018412618));
#51466=CARTESIAN_POINT('Ctrl Pts',(-26.5375922744891,24.759370680268,22.2313134539935));
#51467=CARTESIAN_POINT('Ctrl Pts',(-26.5349894552735,24.7657816077551,22.2309002362025));
#51468=CARTESIAN_POINT('Ctrl Pts',(-26.4200259315163,25.0463490829511,22.2128349712719));
#51469=CARTESIAN_POINT('Ctrl Pts',(-26.2704015828963,25.3037473879628,22.1969372140797));
#51470=CARTESIAN_POINT('Ctrl Pts',(-26.0468996287055,25.5891854542539,22.1763516665697));
#51471=CARTESIAN_POINT('Ctrl Pts',(-26.0045214351048,25.6400031597028,22.1725600827292));
#51472=CARTESIAN_POINT('Ctrl Pts',(-25.8916453247069,25.7671855340542,22.1626787989449));
#51473=CARTESIAN_POINT('Ctrl Pts',(-25.8189688593733,25.8415043470074,22.1565164668457));
#51474=CARTESIAN_POINT('Ctrl Pts',(-25.7356932462003,25.9188093557424,22.1495976288782));
#51475=CARTESIAN_POINT('Ctrl Pts',(-25.7285205692205,25.9254074526995,22.1490028155607));
#51476=CARTESIAN_POINT('Ctrl Pts',(-25.7186909424206,25.9343676838472,22.1481891427955));
#51477=CARTESIAN_POINT('Ctrl Pts',(-25.7160597971692,25.9367581546699,22.1479714861979));
#51478=CARTESIAN_POINT('Ctrl Pts',(-25.7111028751142,25.9412467113325,22.147561700278));
#51479=CARTESIAN_POINT('Ctrl Pts',(-25.7087779824436,25.9433457710143,22.1473696124448));
#51480=CARTESIAN_POINT('Ctrl Pts',(-25.7039281465232,25.9477116914328,22.146969134353));
#51481=CARTESIAN_POINT('Ctrl Pts',(-25.7014026770027,25.9499779594717,22.1467607194577));
#51482=CARTESIAN_POINT('Ctrl Pts',(-25.6955711712917,25.9551943460036,22.1462797634256));
#51483=CARTESIAN_POINT('Ctrl Pts',(-25.6922626262953,25.9581416383459,22.146007103989));
#51484=CARTESIAN_POINT('Ctrl Pts',(-25.6819471750358,25.9672926830953,22.1451576581534));
#51485=CARTESIAN_POINT('Ctrl Pts',(-25.6749193639823,25.9734727022002,22.1445798800348));
#51486=CARTESIAN_POINT('Ctrl Pts',(-25.6150691058854,26.0256424703571,22.1396671598498));
#51487=CARTESIAN_POINT('Ctrl Pts',(-25.5607909471644,26.0699264928203,22.1352621883468));
#51488=CARTESIAN_POINT('Ctrl Pts',(-25.4983860074865,26.1175400489098,22.1302467216276));
#51489=CARTESIAN_POINT('Ctrl Pts',(-25.491635210435,26.1226487935692,22.1297047946656));
#51490=CARTESIAN_POINT('Ctrl Pts',(-25.4406261694151,26.1609353220647,22.1256147324813));
#51491=CARTESIAN_POINT('Ctrl Pts',(-25.3955425824739,26.1929937582597,22.1220263236932));
#51492=CARTESIAN_POINT('Ctrl Pts',(-25.2653797843378,26.2805961476516,22.1117435424544));
#51493=CARTESIAN_POINT('Ctrl Pts',(-25.1784720266675,26.3332969913784,22.1049664811489));
#51494=CARTESIAN_POINT('Ctrl Pts',(-25.0188393391407,26.420058829961,22.0927325718472));
#51495=CARTESIAN_POINT('Ctrl Pts',(-24.9470512685393,26.4556764865226,22.0873041555619));
#51496=CARTESIAN_POINT('Ctrl Pts',(-24.7076038378035,26.5635509810317,22.0695337636006));
#51497=CARTESIAN_POINT('Ctrl Pts',(-24.5351064127702,26.6242578645162,22.0572397142614));
#51498=CARTESIAN_POINT('Ctrl Pts',(-24.3429870226977,26.6740230712446,22.0446866660121));
#51499=CARTESIAN_POINT('Ctrl Pts',(-24.327565822985,26.6778961221649,22.0436869416211));
#51500=CARTESIAN_POINT('Ctrl Pts',(-24.3084697326305,26.6825421611258,22.0424592612208));
#51501=CARTESIAN_POINT('Ctrl Pts',(-24.3048216792032,26.6834229784477,22.0422251917254));
#51502=CARTESIAN_POINT('Ctrl Pts',(-24.299079549773,26.6847987970287,22.041857496811));
#51503=CARTESIAN_POINT('Ctrl Pts',(-24.2969865171199,26.6852980732459,22.0417236241302));
#51504=CARTESIAN_POINT('Ctrl Pts',(-24.2930770145456,26.6862265165814,22.0414738572342));
#51505=CARTESIAN_POINT('Ctrl Pts',(-24.2912606839137,26.686656199047,22.0413579338199));
#51506=CARTESIAN_POINT('Ctrl Pts',(-24.2871867342965,26.6876162214126,22.0410981836099));
#51507=CARTESIAN_POINT('Ctrl Pts',(-24.2849289205212,26.6881457013736,22.0409544074057));
#51508=CARTESIAN_POINT('Ctrl Pts',(-24.2791973384445,26.6894832895775,22.0405898742143));
#51509=CARTESIAN_POINT('Ctrl Pts',(-24.2757227863422,26.690288071689,22.0403693096189));
#51510=CARTESIAN_POINT('Ctrl Pts',(-24.2566864008831,26.6946640305572,22.0391631416016));
#51511=CARTESIAN_POINT('Ctrl Pts',(-24.2410991703837,26.6981253741572,22.0381837897782));
#51512=CARTESIAN_POINT('Ctrl Pts',(-23.9414990950949,26.7623228128117,22.0195070594619));
#51513=CARTESIAN_POINT('Ctrl Pts',(-23.6505361469162,26.7845184406953,22.003818444791));
#51514=CARTESIAN_POINT('Ctrl Pts',(-23.2366850760106,26.7601085720148,21.9804890889904));
#51515=CARTESIAN_POINT('Ctrl Pts',(-23.1134062222116,26.7456651514575,21.9734238939847));
#51516=CARTESIAN_POINT('Ctrl Pts',(-22.9355066728671,26.7143340014971,21.9628353624472));
#51517=CARTESIAN_POINT('Ctrl Pts',(-22.8800106240596,26.7030448227496,21.9594763885099));
#51518=CARTESIAN_POINT('Ctrl Pts',(-22.8050670341939,26.6857314588107,21.9548507690711));
#51519=CARTESIAN_POINT('Ctrl Pts',(-22.7853349179991,26.6809761770409,21.9536243836975));
#51520=CARTESIAN_POINT('Ctrl Pts',(-22.7520677239213,26.6726257730871,21.9515417922851));
#51521=CARTESIAN_POINT('Ctrl Pts',(-22.7385086078025,26.6691282006269,21.950688737525));
#51522=CARTESIAN_POINT('Ctrl Pts',(-22.7199581736282,26.6642139562409,21.9495157190235));
#51523=CARTESIAN_POINT('Ctrl Pts',(-22.7149467039351,26.6628733965306,21.9491982277253));
#51524=CARTESIAN_POINT('Ctrl Pts',(-22.7069145331746,26.6607040092595,21.9486884022618));
#51525=CARTESIAN_POINT('Ctrl Pts',(-22.7038917512611,26.6598828639475,21.9484963181619));
#51526=CARTESIAN_POINT('Ctrl Pts',(-22.6976040867666,26.6581649589556,21.9480963070609));
#51527=CARTESIAN_POINT('Ctrl Pts',(-22.694339412041,26.6572674588597,21.9478883561636));
#51528=CARTESIAN_POINT('Ctrl Pts',(-22.6868502574631,26.6551958967247,21.9474107232927));
#51529=CARTESIAN_POINT('Ctrl Pts',(-22.6826267540049,26.6540183567493,21.9471409282481));
#51530=CARTESIAN_POINT('Ctrl Pts',(-22.6692905905609,26.650270800429,21.9462876405822));
#51531=CARTESIAN_POINT('Ctrl Pts',(-22.6601869089148,26.6476692605655,21.9457031201806));
#51532=CARTESIAN_POINT('Ctrl Pts',(-22.5841290690265,26.6255713748685,21.9408023910844));
#51533=CARTESIAN_POINT('Ctrl Pts',(-22.5178170233325,26.6039480348988,21.9364167986947));
#51534=CARTESIAN_POINT('Ctrl Pts',(-22.4455299461476,26.5777526307021,21.9315047403781));
#51535=CARTESIAN_POINT('Ctrl Pts',(-22.4388056917508,26.5752905085064,21.9310465493669));
#51536=CARTESIAN_POINT('Ctrl Pts',(-22.4063475737677,26.5632829592691,21.9288287311217));
#51537=CARTESIAN_POINT('Ctrl Pts',(-22.380728739186,26.553431670277,21.9270595885942));
#51538=CARTESIAN_POINT('Ctrl Pts',(-22.2598109093321,26.505152923231,21.9186208491186));
#51539=CARTESIAN_POINT('Ctrl Pts',(-22.1663048046482,26.4625273153929,21.9118293256875));
#51540=CARTESIAN_POINT('Ctrl Pts',(-22.0750357484432,26.415536637139,21.9049549578222));
#51541=CARTESIAN_POINT('Ctrl Pts',(-22.075036015355,26.4155367745608,21.6601868380444));
#51542=CARTESIAN_POINT('Ctrl Pts',(-22.0764463957423,26.4162629211716,21.6602862264009));
#51543=CARTESIAN_POINT('Ctrl Pts',(-22.0778573206843,26.4169880307625,21.6603855517639));
#51544=CARTESIAN_POINT('Ctrl Pts',(-22.0836622160409,26.4199658954842,21.6607937824192));
#51545=CARTESIAN_POINT('Ctrl Pts',(-22.0880608519347,26.4222096060075,21.6611021319279));
#51546=CARTESIAN_POINT('Ctrl Pts',(-22.0946247348677,26.4255388036736,21.6615607807606));
#51547=CARTESIAN_POINT('Ctrl Pts',(-22.0967860507001,26.4266319603244,21.6617115621373));
#51548=CARTESIAN_POINT('Ctrl Pts',(-22.1004690787101,26.4284895618734,21.6619680930338));
#51549=CARTESIAN_POINT('Ctrl Pts',(-22.1019901646428,26.4292552372642,21.6620739207706));
#51550=CARTESIAN_POINT('Ctrl Pts',(-22.1051081026874,26.4308216304759,21.6622906026426));
#51551=CARTESIAN_POINT('Ctrl Pts',(-22.1067050103529,26.4316222246031,21.6624014488298));
#51552=CARTESIAN_POINT('Ctrl Pts',(-22.1105396657435,26.4335407037762,21.662667310779));
#51553=CARTESIAN_POINT('Ctrl Pts',(-22.1127780551258,26.4346573141347,21.6628222457602));
#51554=CARTESIAN_POINT('Ctrl Pts',(-22.1208909778117,26.4386926192767,21.6633828819819));
#51555=CARTESIAN_POINT('Ctrl Pts',(-22.1267731707987,26.4415960087239,21.6637876251807));
#51556=CARTESIAN_POINT('Ctrl Pts',(-22.2222988582826,26.4883843241016,21.6703330560544));
#51557=CARTESIAN_POINT('Ctrl Pts',(-22.3139353039589,26.5281047299056,21.6762200766067));
#51558=CARTESIAN_POINT('Ctrl Pts',(-22.620989974494,26.6445752253522,21.6951494157109));
#51559=CARTESIAN_POINT('Ctrl Pts',(-22.8427289817234,26.7026778028909,21.7076145565472));
#51560=CARTESIAN_POINT('Ctrl Pts',(-23.2295927045337,26.7611328033801,21.7297671697963));
#51561=CARTESIAN_POINT('Ctrl Pts',(-23.3920115749825,26.7732207244189,21.7391768018782));
#51562=CARTESIAN_POINT('Ctrl Pts',(-23.5783271758149,26.7729673299021,21.7504254247219));
#51563=CARTESIAN_POINT('Ctrl Pts',(-23.6020172087237,26.7726738616832,21.751863735977));
#51564=CARTESIAN_POINT('Ctrl Pts',(-23.6320087835959,26.7719715267369,21.753695485374));
#51565=CARTESIAN_POINT('Ctrl Pts',(-23.6383157110017,26.7718053006707,21.7540812910625));
#51566=CARTESIAN_POINT('Ctrl Pts',(-23.6484193885904,26.7715093147956,21.754700337127));
#51567=CARTESIAN_POINT('Ctrl Pts',(-23.6522164901239,26.7713913591052,21.7549332064639));
#51568=CARTESIAN_POINT('Ctrl Pts',(-23.659362594924,26.7711567193504,21.7553718877046));
#51569=CARTESIAN_POINT('Ctrl Pts',(-23.6627116448107,26.7710415250468,21.7555776525232));
#51570=CARTESIAN_POINT('Ctrl Pts',(-23.6702323417442,26.7707710977727,21.7560401183406));
#51571=CARTESIAN_POINT('Ctrl Pts',(-23.6744038734137,26.7706129825387,21.7562969095734));
#51572=CARTESIAN_POINT('Ctrl Pts',(-23.6849974750038,26.7701908347571,21.7569497314156));
#51573=CARTESIAN_POINT('Ctrl Pts',(-23.6914190618763,26.7699156949888,21.7573461104819));
#51574=CARTESIAN_POINT('Ctrl Pts',(-23.7267928537196,26.7682940356877,21.7595332403863));
#51575=CARTESIAN_POINT('Ctrl Pts',(-23.7557259436035,26.7665762397858,21.7613356246155));
#51576=CARTESIAN_POINT('Ctrl Pts',(-24.1039121620295,26.7411867143453,21.7831950315176));
#51577=CARTESIAN_POINT('Ctrl Pts',(-24.4178817536088,26.6704642075102,21.8048908056952));
#51578=CARTESIAN_POINT('Ctrl Pts',(-24.7931749678692,26.5248250988597,21.8320557341972));
#51579=CARTESIAN_POINT('Ctrl Pts',(-24.8689946044561,26.4919967141221,21.8375958184617));
#51580=CARTESIAN_POINT('Ctrl Pts',(-25.0116412155515,26.4236087082552,21.8480249947163));
#51581=CARTESIAN_POINT('Ctrl Pts',(-25.0786452988882,26.3885355095655,21.8529262326549));
#51582=CARTESIAN_POINT('Ctrl Pts',(-25.1510769983085,26.3473114039068,21.8581780833967));
#51583=CARTESIAN_POINT('Ctrl Pts',(-25.1577809798753,26.3434638732673,21.8586637204735));
#51584=CARTESIAN_POINT('Ctrl Pts',(-25.169324016705,26.3367838031091,21.859499029815));
#51585=CARTESIAN_POINT('Ctrl Pts',(-25.1741696056248,26.333962706671,21.8598494141207));
#51586=CARTESIAN_POINT('Ctrl Pts',(-25.181267489776,26.3298054861363,21.8603622431474));
#51587=CARTESIAN_POINT('Ctrl Pts',(-25.1835255245471,26.3284792594774,21.8605253260132));
#51588=CARTESIAN_POINT('Ctrl Pts',(-25.1874251810291,26.326182450778,21.8608068610967));
#51589=CARTESIAN_POINT('Ctrl Pts',(-25.1890675599506,26.3252131625194,21.8609253982015));
#51590=CARTESIAN_POINT('Ctrl Pts',(-25.1922267036798,26.3233449372324,21.8611533392096));
#51591=CARTESIAN_POINT('Ctrl Pts',(-25.1937435881581,26.3224462151301,21.8612627569666));
#51592=CARTESIAN_POINT('Ctrl Pts',(-25.1973351823327,26.3203142872611,21.86152176174));
#51593=CARTESIAN_POINT('Ctrl Pts',(-25.1994092492966,26.319079992654,21.8616712771367));
#51594=CARTESIAN_POINT('Ctrl Pts',(-25.2066647924874,26.3147511135016,21.8621941322118));
#51595=CARTESIAN_POINT('Ctrl Pts',(-25.2118390024339,26.3116442801015,21.8625666738927));
#51596=CARTESIAN_POINT('Ctrl Pts',(-25.276409863679,26.2726257663442,21.8672120642953));
#51597=CARTESIAN_POINT('Ctrl Pts',(-25.334645386931,26.2348156267273,21.8713625910134));
#51598=CARTESIAN_POINT('Ctrl Pts',(-25.4469352331633,26.1566399255117,21.8793814423341));
#51599=CARTESIAN_POINT('Ctrl Pts',(-25.5010325856955,26.1164011350829,21.8832524784931));
#51600=CARTESIAN_POINT('Ctrl Pts',(-25.6139967911004,26.026737493405,21.8914431122713));
#51601=CARTESIAN_POINT('Ctrl Pts',(-25.6724377510352,25.976844511764,21.895747409662));
#51602=CARTESIAN_POINT('Ctrl Pts',(-25.846438005017,25.8171962918457,21.9089509044041));
#51603=CARTESIAN_POINT('Ctrl Pts',(-25.9556824584759,25.7009281309257,21.9178122560498));
#51604=CARTESIAN_POINT('Ctrl Pts',(-26.1411737756435,25.4716165068541,21.9347404042038));
#51605=CARTESIAN_POINT('Ctrl Pts',(-26.2197192339311,25.360902340441,21.9427102115787));
#51606=CARTESIAN_POINT('Ctrl Pts',(-26.2965810997774,25.2366414030097,21.9516028868877));
#51607=CARTESIAN_POINT('Ctrl Pts',(-26.3020662368156,25.2276759598599,21.9522441632564));
#51608=CARTESIAN_POINT('Ctrl Pts',(-26.3099024106677,25.2147258749448,21.9531700353776));
#51609=CARTESIAN_POINT('Ctrl Pts',(-26.3122889169085,25.2107626856255,21.953453329523));
#51610=CARTESIAN_POINT('Ctrl Pts',(-26.3164212021051,25.2038667847388,21.9539461666776));
#51611=CARTESIAN_POINT('Ctrl Pts',(-26.3181708756185,25.2009364058075,21.9541555668586));
#51612=CARTESIAN_POINT('Ctrl Pts',(-26.3215299043653,25.1952902976599,21.9545589762894));
#51613=CARTESIAN_POINT('Ctrl Pts',(-26.3231399317027,25.1925749709514,21.9547529607105));
#51614=CARTESIAN_POINT('Ctrl Pts',(-26.3269290013617,25.1861632129859,21.9552109676479));
#51615=CARTESIAN_POINT('Ctrl Pts',(-26.3291046522654,25.1824647930407,21.9554751133619));
#51616=CARTESIAN_POINT('Ctrl Pts',(-26.3366292032537,25.1696150495754,21.9563927235673));
#51617=CARTESIAN_POINT('Ctrl Pts',(-26.3419402915647,25.1604417650476,21.9570475593227));
#51618=CARTESIAN_POINT('Ctrl Pts',(-26.4051572237718,25.0500008402285,21.9649289668725));
#51619=CARTESIAN_POINT('Ctrl Pts',(-26.457561940388,24.9456994672812,21.9723527171089));
#51620=CARTESIAN_POINT('Ctrl Pts',(-26.6106377890003,24.5947787639318,21.9973047179695));
#51621=CARTESIAN_POINT('Ctrl Pts',(-26.6864262812096,24.3385247782045,22.0155850818417));
#51622=CARTESIAN_POINT('Ctrl Pts',(-26.7434208645225,23.99378934334,22.0389717183269));
#51623=CARTESIAN_POINT('Ctrl Pts',(-26.753813932362,23.9111477523414,22.0444796083276));
#51624=CARTESIAN_POINT('Ctrl Pts',(-26.7648017569625,23.7842163582056,22.0527043200266));
#51625=CARTESIAN_POINT('Ctrl Pts',(-26.7677048295803,23.7401656530567,22.0555154931734));
#51626=CARTESIAN_POINT('Ctrl Pts',(-26.7699243108141,23.6911613928198,22.0585846933093));
#51627=CARTESIAN_POINT('Ctrl Pts',(-26.7701352643545,23.6862556973999,22.058891296807));
#51628=CARTESIAN_POINT('Ctrl Pts',(-26.7704324939789,23.6789549648665,22.0593466076058));
#51629=CARTESIAN_POINT('Ctrl Pts',(-26.7705273104283,23.6765603119111,22.0594957932674));
#51630=CARTESIAN_POINT('Ctrl Pts',(-26.7706847786253,23.6724678816208,22.059750478599));
#51631=CARTESIAN_POINT('Ctrl Pts',(-26.7707487589792,23.6707701608151,22.0598560535757));
#51632=CARTESIAN_POINT('Ctrl Pts',(-26.7708775871916,23.6672783296955,22.0600730329025));
#51633=CARTESIAN_POINT('Ctrl Pts',(-26.770942278251,23.6654842198546,22.0601844280769));
#51634=CARTESIAN_POINT('Ctrl Pts',(-26.7711127108691,23.6606452445706,22.060484638638));
#51635=CARTESIAN_POINT('Ctrl Pts',(-26.7712156342006,23.6576002718945,22.0606732944818));
#51636=CARTESIAN_POINT('Ctrl Pts',(-26.771578787329,23.646385417128,22.0613672049864));
#51637=CARTESIAN_POINT('Ctrl Pts',(-26.7718122553643,23.6382146096634,22.0618709643138));
#51638=CARTESIAN_POINT('Ctrl Pts',(-26.7722333698154,23.6212109205243,22.0629157143172));
#51639=CARTESIAN_POINT('Ctrl Pts',(-26.7724157877892,23.6123779642503,22.0634564197166));
#51640=CARTESIAN_POINT('Ctrl Pts',(-26.7726931806226,23.5956052742367,22.0644795172046));
#51641=CARTESIAN_POINT('Ctrl Pts',(-26.7727951398391,23.5876657472716,22.0649622648359));
#51642=CARTESIAN_POINT('Ctrl Pts',(-26.7729146745632,23.5745958028931,22.0657545310933));
#51643=CARTESIAN_POINT('Ctrl Pts',(-26.7729493432903,23.5694656308423,22.0660648935312));
#51644=CARTESIAN_POINT('Ctrl Pts',(-26.7729909304081,23.5599488226589,22.0666395309106));
#51645=CARTESIAN_POINT('Ctrl Pts',(-26.7730011430885,23.5555622220122,22.0669039639632));
#51646=CARTESIAN_POINT('Ctrl Pts',(-26.7730295122418,23.4565144897036,22.0728651960129));
#51647=CARTESIAN_POINT('Ctrl Pts',(-26.768885907985,23.3618891241273,22.0783635827235));
#51648=CARTESIAN_POINT('Ctrl Pts',(-26.7342660432386,22.968715485987,22.1008848756491));
#51649=CARTESIAN_POINT('Ctrl Pts',(-26.6663520468112,22.6750025033421,22.1170727569472));
#51650=CARTESIAN_POINT('Ctrl Pts',(-26.5512600840379,22.3753004133235,22.1358665854907));
#51651=CARTESIAN_POINT('Ctrl Pts',(-26.5435381406761,22.3557651751386,22.1371017100258));
#51652=CARTESIAN_POINT('Ctrl Pts',(-26.5298601922505,22.3221279270264,22.1392469360055));
#51653=CARTESIAN_POINT('Ctrl Pts',(-26.5239936182054,22.3079901622655,22.1401542789479));
#51654=CARTESIAN_POINT('Ctrl Pts',(-26.5153525377084,22.287578160092,22.1414728608592));
#51655=CARTESIAN_POINT('Ctrl Pts',(-26.5126583080729,22.2812700143222,22.1418815481744));
#51656=CARTESIAN_POINT('Ctrl Pts',(-26.4920611999013,22.2334679706731,22.1449876893229));
#51657=CARTESIAN_POINT('Ctrl Pts',(-26.4733081822191,22.1923478333727,22.1477123276043));
#51658=CARTESIAN_POINT('Ctrl Pts',(-26.4504517596974,22.1448992187652,22.1509229178505));
#51659=CARTESIAN_POINT('Ctrl Pts',(-26.4471826340804,22.1381726909365,22.1513796441832));
#51660=CARTESIAN_POINT('Ctrl Pts',(-26.4419325875747,22.1274652009284,22.1521092198527));
#51661=CARTESIAN_POINT('Ctrl Pts',(-26.4399667768313,22.1234768256693,22.1523815406841));
#51662=CARTESIAN_POINT('Ctrl Pts',(-26.4364850672209,22.116449600351,22.1528623529357));
#51663=CARTESIAN_POINT('Ctrl Pts',(-26.434972604284,22.1134090476228,22.1530707236677));
#51664=CARTESIAN_POINT('Ctrl Pts',(-26.4318379943147,22.1071323398165,22.1535015588974));
#51665=CARTESIAN_POINT('Ctrl Pts',(-26.4302151956256,22.1038965171593,22.1537240460665));
#51666=CARTESIAN_POINT('Ctrl Pts',(-26.4260517117564,22.0956294164649,22.1542934458337));
#51667=CARTESIAN_POINT('Ctrl Pts',(-26.4235032807951,22.09060207232,22.1546406307176));
#51668=CARTESIAN_POINT('Ctrl Pts',(-26.4130917608197,22.0701959632868,22.1560536467266));
#51669=CARTESIAN_POINT('Ctrl Pts',(-26.4051183990443,22.054874065133,22.1571233653697));
#51670=CARTESIAN_POINT('Ctrl Pts',(-26.3523250843868,21.9553858452228,22.1641274728358));
#51671=CARTESIAN_POINT('Ctrl Pts',(-26.303915742813,21.8731877842,22.1701896900044));
#51672=CARTESIAN_POINT('Ctrl Pts',(-26.1736907060326,21.6729435324092,22.1856814210099));
#51673=CARTESIAN_POINT('Ctrl Pts',(-26.0875011981096,21.5579979234275,22.1952531613907));
#51674=CARTESIAN_POINT('Ctrl Pts',(-25.8311015538655,21.2597858334105,22.2217891022904));
#51675=CARTESIAN_POINT('Ctrl Pts',(-25.6467759527366,21.0899435887018,22.2389369743643));
#51676=CARTESIAN_POINT('Ctrl Pts',(-25.4430266605609,20.9418952352266,22.2548551913077));
#51677=CARTESIAN_POINT('Ctrl Pts',(-25.4413821789678,20.9407026957653,22.2549834827015));
#51678=CARTESIAN_POINT('Ctrl Pts',(-25.4292130626363,20.9318954825739,22.2559314527651));
#51679=CARTESIAN_POINT('Ctrl Pts',(-25.4186433916031,20.9243427994723,22.2567471864274));
#51680=CARTESIAN_POINT('Ctrl Pts',(-25.4050658896473,20.9147643204457,22.257785019326));
#51681=CARTESIAN_POINT('Ctrl Pts',(-25.4021001084835,20.9126795455725,22.2580111084077));
#51682=CARTESIAN_POINT('Ctrl Pts',(-25.3973743609445,20.9093695147847,22.2583703887834));
#51683=CARTESIAN_POINT('Ctrl Pts',(-25.3956166896726,20.908141011412,22.2585038035544));
#51684=CARTESIAN_POINT('Ctrl Pts',(-25.3923261746684,20.9058460305471,22.258753165245));
#51685=CARTESIAN_POINT('Ctrl Pts',(-25.3907936406341,20.9047791381826,22.2588691404284));
#51686=CARTESIAN_POINT('Ctrl Pts',(-25.3873472344706,20.9023843246763,22.2591295829135));
#51687=CARTESIAN_POINT('Ctrl Pts',(-25.385432853435,20.9010571490387,22.25927399844));
#51688=CARTESIAN_POINT('Ctrl Pts',(-25.3797503594922,20.8971267834943,22.259701925648));
#51689=CARTESIAN_POINT('Ctrl Pts',(-25.3759781142735,20.894529534955,22.2599850301324));
#51690=CARTESIAN_POINT('Ctrl Pts',(-25.3457506897403,20.8738123336755,22.2622459460249));
#51691=CARTESIAN_POINT('Ctrl Pts',(-25.3190307501819,20.8560792682073,22.2641978257712));
#51692=CARTESIAN_POINT('Ctrl Pts',(-25.2238382042374,20.7949301824093,22.2710052571156));
#51693=CARTESIAN_POINT('Ctrl Pts',(-25.1539921504694,20.7536990013019,22.2757378331628));
#51694=CARTESIAN_POINT('Ctrl Pts',(-24.7428921853354,20.5314950188285,22.3025486803452));
#51695=CARTESIAN_POINT('Ctrl Pts',(-24.3729023624256,20.4104169822941,22.3230909516774));
#51696=CARTESIAN_POINT('Ctrl Pts',(-23.9707885972029,20.3549977687582,22.3476492421347));
#51697=CARTESIAN_POINT('Ctrl Pts',(-23.9513014058937,20.3524934168825,22.3488434309341));
#51698=CARTESIAN_POINT('Ctrl Pts',(-23.9256729575317,20.3494377835366,22.3504196515478));
#51699=CARTESIAN_POINT('Ctrl Pts',(-23.9195510050214,20.348725679562,22.3507965941183));
#51700=CARTESIAN_POINT('Ctrl Pts',(-23.910084729048,20.3476520778044,22.3513801241917));
#51701=CARTESIAN_POINT('Ctrl Pts',(-23.9067417958936,20.3472782448974,22.3515863218109));
#51702=CARTESIAN_POINT('Ctrl Pts',(-23.9000738679614,20.3465431532836,22.351997870356));
#51703=CARTESIAN_POINT('Ctrl Pts',(-23.8967488837817,20.3461818354579,22.3522032191456));
#51704=CARTESIAN_POINT('Ctrl Pts',(-23.8894444222316,20.3453995807216,22.352654623136));
#51705=CARTESIAN_POINT('Ctrl Pts',(-23.8854647155961,20.3449808790105,22.3529007485635));
#51706=CARTESIAN_POINT('Ctrl Pts',(-23.874064582173,20.3438029441067,22.3536063291968));
#51707=CARTESIAN_POINT('Ctrl Pts',(-23.8666423218697,20.3430620632392,22.3540663627267));
#51708=CARTESIAN_POINT('Ctrl Pts',(-23.8499599849756,20.3414553265864,22.3551018306533));
#51709=CARTESIAN_POINT('Ctrl Pts',(-23.8406986267633,20.3406037777024,22.3556777130099));
#51710=CARTESIAN_POINT('Ctrl Pts',(-23.6115287247441,20.3205324242405,22.3699538155614));
#51711=CARTESIAN_POINT('Ctrl Pts',(-23.3902729610331,20.3239206420583,22.3843927214189));
#51712=CARTESIAN_POINT('Ctrl Pts',(-22.9177362731837,20.3798968808219,22.4163855404536));
#51713=CARTESIAN_POINT('Ctrl Pts',(-22.6687886155403,20.4399045165147,22.4339703003795));
#51714=CARTESIAN_POINT('Ctrl Pts',(-22.4265410283983,20.5297558656829,22.4505030017711));
#51715=CARTESIAN_POINT('Ctrl Pts',(-22.4235645046418,20.5308648881647,22.450706036401));
#51716=CARTESIAN_POINT('Ctrl Pts',(-22.4147919680841,20.5341482244502,22.4513041101213));
#51717=CARTESIAN_POINT('Ctrl Pts',(-22.4090005361102,20.5363348540477,22.4516985345263));
#51718=CARTESIAN_POINT('Ctrl Pts',(-22.3829131339263,20.5462704640352,22.4534732452903));
#51719=CARTESIAN_POINT('Ctrl Pts',(-22.3626889078704,20.5542081004693,22.4548437116512));
#51720=CARTESIAN_POINT('Ctrl Pts',(-22.3388628863324,20.5638385500347,22.4564505521771));
#51721=CARTESIAN_POINT('Ctrl Pts',(-22.3351826613638,20.5653340146556,22.4566985301896));
#51722=CARTESIAN_POINT('Ctrl Pts',(-22.3292671729498,20.5677505349162,22.4570967602308));
#51723=CARTESIAN_POINT('Ctrl Pts',(-22.327030179076,20.568667301787,22.4572472708386));
#51724=CARTESIAN_POINT('Ctrl Pts',(-22.323054038676,20.5703020352439,22.4575146441724));
#51725=CARTESIAN_POINT('Ctrl Pts',(-22.3213144889652,20.5710190078216,22.4576315675245));
#51726=CARTESIAN_POINT('Ctrl Pts',(-22.3176647016531,20.5725270442687,22.457876777482));
#51727=CARTESIAN_POINT('Ctrl Pts',(-22.3157546015942,20.5733184212602,22.4580050443085));
#51728=CARTESIAN_POINT('Ctrl Pts',(-22.3107279646035,20.5754066861511,22.4583424306366));
#51729=CARTESIAN_POINT('Ctrl Pts',(-22.3076126908925,20.5767066377375,22.4585513629225));
#51730=CARTESIAN_POINT('Ctrl Pts',(-22.2937098885428,20.5825337085041,22.4594830753684));
#51731=CARTESIAN_POINT('Ctrl Pts',(-22.2829448372896,20.5871147277434,22.460202602816));
#51732=CARTESIAN_POINT('Ctrl Pts',(-22.20265050817,20.621801241231,22.4655568614164));
#51733=CARTESIAN_POINT('Ctrl Pts',(-22.1341710248566,20.6542944127737,22.4700528257604));
#51734=CARTESIAN_POINT('Ctrl Pts',(-21.9935433494579,20.7272043907029,22.4792657272348));
#51735=CARTESIAN_POINT('Ctrl Pts',(-21.9216773645678,20.7680432170251,22.4839626674951));
#51736=CARTESIAN_POINT('Ctrl Pts',(-21.5793422268877,20.9803949539836,22.5066513606238));
#51737=CARTESIAN_POINT('Ctrl Pts',(-21.3339326999549,21.1887762136587,22.5241234346838));
#51738=CARTESIAN_POINT('Ctrl Pts',(-21.104402099322,21.4515016581899,22.5451230954145));
#51739=CARTESIAN_POINT('Ctrl Pts',(-21.0858283122358,21.4733431087205,22.5468604336561));
#51740=CARTESIAN_POINT('Ctrl Pts',(-21.0634670352489,21.5003607196851,22.5490004411722));
#51741=CARTESIAN_POINT('Ctrl Pts',(-21.0593999425179,21.5053046290978,22.5493916717176));
#51742=CARTESIAN_POINT('Ctrl Pts',(-21.0527102191427,21.5134861436145,22.5500385186929));
#51743=CARTESIAN_POINT('Ctrl Pts',(-21.0500790751915,21.5167167907402,22.5502937897018));
#51744=CARTESIAN_POINT('Ctrl Pts',(-21.0453435231106,21.5225544165647,22.5507547856067));
#51745=CARTESIAN_POINT('Ctrl Pts',(-21.0432368978333,21.5251595958453,22.5509604205573));
#51746=CARTESIAN_POINT('Ctrl Pts',(-21.0387952470279,21.5306699604002,22.5513951720596));
#51747=CARTESIAN_POINT('Ctrl Pts',(-21.0364611928579,21.5335759191499,22.5516243272984));
#51748=CARTESIAN_POINT('Ctrl Pts',(-21.030277491015,21.5413022057085,22.5522332949957));
#51749=CARTESIAN_POINT('Ctrl Pts',(-21.0264366474953,21.5461295315411,22.5526134600353));
#51750=CARTESIAN_POINT('Ctrl Pts',(-21.0180051220917,21.5567892863216,22.5534522708849));
#51751=CARTESIAN_POINT('Ctrl Pts',(-21.0134206914014,21.5626265943797,22.5539111640394));
#51752=CARTESIAN_POINT('Ctrl Pts',(-20.9998741074977,21.5799985318516,22.5552755638564));
#51753=CARTESIAN_POINT('Ctrl Pts',(-20.9909702570987,21.5915781947735,22.5561833777106));
#51754=CARTESIAN_POINT('Ctrl Pts',(-20.895514836192,21.7174823367168,22.5660368682417));
#51755=CARTESIAN_POINT('Ctrl Pts',(-20.8166189757819,21.8373846882711,22.575280703499));
#51756=CARTESIAN_POINT('Ctrl Pts',(-20.6608902327134,22.1123670395073,22.5961746626137));
#51757=CARTESIAN_POINT('Ctrl Pts',(-20.5880219296622,22.2691939063896,22.6079032353554));
#51758=CARTESIAN_POINT('Ctrl Pts',(-20.4766736586584,22.5698777183794,22.6295715035838));
#51759=CARTESIAN_POINT('Ctrl Pts',(-20.434893406036,22.71205890173,22.6394965467774));
#51760=CARTESIAN_POINT('Ctrl Pts',(-20.4020508637683,22.8610757589922,22.6492677469313));
#51761=CARTESIAN_POINT('Ctrl Pts',(-20.4010786351739,22.8655320515275,22.6495593719663));
#51762=CARTESIAN_POINT('Ctrl Pts',(-20.3990084568063,22.8751185692532,22.6501854589494));
#51763=CARTESIAN_POINT('Ctrl Pts',(-20.3979135647258,22.8802494533953,22.6505197738264));
#51764=CARTESIAN_POINT('Ctrl Pts',(-20.3950184359607,22.8939808108006,22.6514123500677));
#51765=CARTESIAN_POINT('Ctrl Pts',(-20.3932408202013,22.9025860836173,22.6519694917124));
#51766=CARTESIAN_POINT('Ctrl Pts',(-20.3886044940821,22.9255027956907,22.6534471070079));
#51767=CARTESIAN_POINT('Ctrl Pts',(-20.3858077197839,22.939826780268,22.654364355876));
#51768=CARTESIAN_POINT('Ctrl Pts',(-20.3824077114731,22.957891911815,22.6555127870491));
#51769=CARTESIAN_POINT('Ctrl Pts',(-20.3817136978569,22.9616154891958,22.6557490533613));
#51770=CARTESIAN_POINT('Ctrl Pts',(-20.3806301746523,22.9674863362381,22.6561208519729));
#51771=CARTESIAN_POINT('Ctrl Pts',(-20.3802362815485,22.9696327777189,22.6562566347933));
#51772=CARTESIAN_POINT('Ctrl Pts',(-20.3795131302459,22.9735961174427,22.65650707372));
#51773=CARTESIAN_POINT('Ctrl Pts',(-20.3791832552723,22.9754128878277,22.6566217646017));
#51774=CARTESIAN_POINT('Ctrl Pts',(-20.3784508956791,22.9794661372953,22.6568774001009));
#51775=CARTESIAN_POINT('Ctrl Pts',(-20.3780492159598,22.9817027537687,22.6570182978256));
#51776=CARTESIAN_POINT('Ctrl Pts',(-20.3768929560307,22.9881803642793,22.6574258908427));
#51777=CARTESIAN_POINT('Ctrl Pts',(-20.3761445089144,22.9924224696903,22.6576922351657));
#51778=CARTESIAN_POINT('Ctrl Pts',(-20.3710763432167,23.0214886722149,22.6595132678774));
#51779=CARTESIAN_POINT('Ctrl Pts',(-20.36703922293,23.0463620852628,22.6610520704653));
#51780=CARTESIAN_POINT('Ctrl Pts',(-20.3555033210215,23.123119164438,22.6657476755412));
#51781=CARTESIAN_POINT('Ctrl Pts',(-20.3489779833575,23.175142717168,22.6688559198228));
#51782=CARTESIAN_POINT('Ctrl Pts',(-20.3361058115589,23.3029499503053,22.6763609012535));
#51783=CARTESIAN_POINT('Ctrl Pts',(-20.3311659639058,23.3788447157707,22.6807055600794));
#51784=CARTESIAN_POINT('Ctrl Pts',(-20.3212907589536,23.7122777360982,22.6995662649293));
#51785=CARTESIAN_POINT('Ctrl Pts',(-20.3445505529016,23.9696824809969,22.7136162244674));
#51786=CARTESIAN_POINT('Ctrl Pts',(-20.419144898918,24.3199234134494,22.734445428303));
#51787=CARTESIAN_POINT('Ctrl Pts',(-20.4446799202941,24.4172264943357,22.7404122811215));
#51788=CARTESIAN_POINT('Ctrl Pts',(-20.4775246203374,24.5221316003617,22.7471030288081));
#51789=CARTESIAN_POINT('Ctrl Pts',(-20.4803694731801,24.5310806233909,22.7476758517431));
#51790=CARTESIAN_POINT('Ctrl Pts',(-20.4846463683445,24.5443335074221,22.7485272701483));
#51791=CARTESIAN_POINT('Ctrl Pts',(-20.4860484686196,24.548647040176,22.7488048782838));
#51792=CARTESIAN_POINT('Ctrl Pts',(-20.4884619394352,24.5560190597004,22.749280166026));
#51793=CARTESIAN_POINT('Ctrl Pts',(-20.489468801106,24.5590790252782,22.7494776965033));
#51794=CARTESIAN_POINT('Ctrl Pts',(-20.4914346141601,24.5650233180399,22.7498619054075));
#51795=CARTESIAN_POINT('Ctrl Pts',(-20.49239306167,24.5679078087575,22.7500485669665));
#51796=CARTESIAN_POINT('Ctrl Pts',(-20.4946652427661,24.5747138470729,22.7504895283489));
#51797=CARTESIAN_POINT('Ctrl Pts',(-20.4959824448376,24.5786342231123,22.7507439428185));
#51798=CARTESIAN_POINT('Ctrl Pts',(-20.4997391659437,24.5897444330355,22.7514661264956));
#51799=CARTESIAN_POINT('Ctrl Pts',(-20.502196539379,24.5969281613456,22.7519344873749));
#51800=CARTESIAN_POINT('Ctrl Pts',(-20.507884945275,24.6133673583722,22.7530095341188));
#51801=CARTESIAN_POINT('Ctrl Pts',(-20.5111328577622,24.6226168679614,22.7536167787485));
#51802=CARTESIAN_POINT('Ctrl Pts',(-20.5215667874341,24.6519028036563,22.7555470498871));
#51803=CARTESIAN_POINT('Ctrl Pts',(-20.5289090218194,24.6718826041495,22.7568752701931));
#51804=CARTESIAN_POINT('Ctrl Pts',(-20.5578279811451,24.7482324784138,22.7619952357672));
#51805=CARTESIAN_POINT('Ctrl Pts',(-20.5807876865711,24.8040620834945,22.7658327958149));
#51806=CARTESIAN_POINT('Ctrl Pts',(-20.6730908106924,25.0117296688887,22.7804700538646));
#51807=CARTESIAN_POINT('Ctrl Pts',(-20.7526188622951,25.1587326170157,22.7915949987556));
#51808=CARTESIAN_POINT('Ctrl Pts',(-20.9757766503871,25.5042045166071,22.8193662535487));
#51809=CARTESIAN_POINT('Ctrl Pts',(-21.1313280487672,25.6937730264392,22.8361182237649));
#51810=CARTESIAN_POINT('Ctrl Pts',(-21.3168358779287,25.8736470160998,22.8524385549815));
#51811=CARTESIAN_POINT('Ctrl Pts',(-21.3269066450529,25.8832859572276,22.8533143698741));
#51812=CARTESIAN_POINT('Ctrl Pts',(-21.3397462274164,25.8954163433241,22.854417789897));
#51813=CARTESIAN_POINT('Ctrl Pts',(-21.3424570464667,25.8979685537831,22.8546500169291));
#51814=CARTESIAN_POINT('Ctrl Pts',(-21.3467528481071,25.901998989989,22.8550168498008));
#51815=CARTESIAN_POINT('Ctrl Pts',(-21.3483348987208,25.9034803144084,22.8551516952708));
#51816=CARTESIAN_POINT('Ctrl Pts',(-21.3512813120622,25.906233562384,22.8554023627709));
#51817=CARTESIAN_POINT('Ctrl Pts',(-21.3526452761006,25.9075058892977,22.8555182159344));
#51818=CARTESIAN_POINT('Ctrl Pts',(-21.3556928342781,25.9103437549952,22.8557766553673));
#51819=CARTESIAN_POINT('Ctrl Pts',(-21.3573769954886,25.9119086731795,22.8559191933721));
#51820=CARTESIAN_POINT('Ctrl Pts',(-21.3623139940557,25.9164862849827,22.8563362121294));
#51821=CARTESIAN_POINT('Ctrl Pts',(-21.3655713923204,25.9194940853371,22.8566103163586));
#51822=CARTESIAN_POINT('Ctrl Pts',(-21.3895337715024,25.9415289113025,22.8586191640723));
#51823=CARTESIAN_POINT('Ctrl Pts',(-21.4104816159046,25.9602917103261,22.8603340449385));
#51824=CARTESIAN_POINT('Ctrl Pts',(-21.4799155573067,26.0208639680878,22.865895127633));
#51825=CARTESIAN_POINT('Ctrl Pts',(-21.5294046982868,26.0615054560786,22.8696664466894));
#51826=CARTESIAN_POINT('Ctrl Pts',(-21.6887799156698,26.1846226042972,22.8813388058313));
#51827=CARTESIAN_POINT('Ctrl Pts',(-21.8027496179665,26.2615666863508,22.8890142787548));
#51828=CARTESIAN_POINT('Ctrl Pts',(-21.9717777561264,26.3605832795733,22.8999608046169));
#51829=CARTESIAN_POINT('Ctrl Pts',(-22.0230465680281,26.3887695579674,22.903226880509));
#51830=CARTESIAN_POINT('Ctrl Pts',(-22.0750361284943,26.4155368328116,22.9065074728514));
#51831=CARTESIAN_POINT('Origin',(-23.5502525316942,23.5502525316942,-77.3107734492734));
#51832=CARTESIAN_POINT('',(-22.0750358518511,26.4155366903795,24.4018187331506));
#51833=CARTESIAN_POINT('',(-22.0750361722079,26.4155368553179,24.1541632309577));
#51834=CARTESIAN_POINT('',(-22.0750360153461,26.4155367745563,-77.3107734492734));
#51835=CARTESIAN_POINT('Ctrl Pts',(-22.0750358518511,26.4155366903795,24.4018187331506));
#51836=CARTESIAN_POINT('Ctrl Pts',(-22.0079631752057,26.3810037345297,24.3975360295522));
#51837=CARTESIAN_POINT('Ctrl Pts',(-21.9420832190341,26.3441054453173,24.3933062394776));
#51838=CARTESIAN_POINT('Ctrl Pts',(-21.7531360000098,26.2293693195608,24.3809461951244));
#51839=CARTESIAN_POINT('Ctrl Pts',(-21.6340112926944,26.1455004915822,24.3728500554956));
#51840=CARTESIAN_POINT('Ctrl Pts',(-21.4157812792204,25.968616138674,24.356803351267));
#51841=CARTESIAN_POINT('Ctrl Pts',(-21.3160859431602,25.8768257411961,24.3488984148019));
#51842=CARTESIAN_POINT('Ctrl Pts',(-21.2076234686032,25.7635458186562,24.3394175410384));
#51843=CARTESIAN_POINT('Ctrl Pts',(-21.192937500504,25.7478976146072,24.3381136787245));
#51844=CARTESIAN_POINT('Ctrl Pts',(-21.1742742557907,25.7276092083621,24.3364300723115));
#51845=CARTESIAN_POINT('Ctrl Pts',(-21.1701521406752,25.7231025018612,24.3360565203686));
#51846=CARTESIAN_POINT('Ctrl Pts',(-21.1635366867497,25.7158284165264,24.3354542655788));
#51847=CARTESIAN_POINT('Ctrl Pts',(-21.1610352777147,25.7130683700349,24.3352259053523));
#51848=CARTESIAN_POINT('Ctrl Pts',(-21.1562843036885,25.7078078609216,24.3347909567144));
#51849=CARTESIAN_POINT('Ctrl Pts',(-21.1540338555843,25.7053081995376,24.3345844060294));
#51850=CARTESIAN_POINT('Ctrl Pts',(-21.148918054092,25.6996079567441,24.3341136702865));
#51851=CARTESIAN_POINT('Ctrl Pts',(-21.1460551830693,25.6964051649177,24.333849381212));
#51852=CARTESIAN_POINT('Ctrl Pts',(-21.1373664027058,25.6866455256547,24.3330446407902));
#51853=CARTESIAN_POINT('Ctrl Pts',(-21.131560886047,25.6800706499723,24.3325033359555));
#51854=CARTESIAN_POINT('Ctrl Pts',(-21.0904037976176,25.6330740364424,24.3286399130351));
#51855=CARTESIAN_POINT('Ctrl Pts',(-21.0560423604432,25.5918000512558,24.3252769939978));
#51856=CARTESIAN_POINT('Ctrl Pts',(-21.0159431835523,25.5411099709902,24.3211788947711));
#51857=CARTESIAN_POINT('Ctrl Pts',(-21.0092005157125,25.5324966798922,24.3204836340995));
#51858=CARTESIAN_POINT('Ctrl Pts',(-20.9853873198502,25.5017558084376,24.3180060720846));
#51859=CARTESIAN_POINT('Ctrl Pts',(-20.9685612876402,25.4794411793467,24.3162146077592));
#51860=CARTESIAN_POINT('Ctrl Pts',(-20.7751902269879,25.2159323113474,24.2951400308635));
#51861=CARTESIAN_POINT('Ctrl Pts',(-20.6327546317516,24.9515405885001,24.2745770975018));
#51862=CARTESIAN_POINT('Ctrl Pts',(-20.4979973178576,24.5883748060967,24.2486904013394));
#51863=CARTESIAN_POINT('Ctrl Pts',(-20.4706223654047,24.5041081209628,24.2428502438269));
#51864=CARTESIAN_POINT('Ctrl Pts',(-20.4406723933143,24.3970923722866,24.2357246382108));
#51865=CARTESIAN_POINT('Ctrl Pts',(-20.4348212558161,24.3753067016134,24.2342889737222));
#51866=CARTESIAN_POINT('Ctrl Pts',(-20.427022506253,24.3450028346687,24.2323143129177));
#51867=CARTESIAN_POINT('Ctrl Pts',(-20.4248802191216,24.3365360351508,24.2317650078408));
#51868=CARTESIAN_POINT('Ctrl Pts',(-20.42172488314,24.3238487769547,24.2309456000024));
#51869=CARTESIAN_POINT('Ctrl Pts',(-20.4206859197852,24.3196348947578,24.2306740574281));
#51870=CARTESIAN_POINT('Ctrl Pts',(-20.4190301628392,24.312860540749,24.2302385143871));
#51871=CARTESIAN_POINT('Ctrl Pts',(-20.4184079944704,24.310301407407,24.2300742084321));
#51872=CARTESIAN_POINT('Ctrl Pts',(-20.4172533017819,24.3055263771203,24.2297680628927));
#51873=CARTESIAN_POINT('Ctrl Pts',(-20.4167199901274,24.3033106750237,24.2296261779976));
#51874=CARTESIAN_POINT('Ctrl Pts',(-20.4157570256761,24.299291197865,24.2293691011349));
#51875=CARTESIAN_POINT('Ctrl Pts',(-20.4153265787939,24.2974876155665,24.2292538629038));
#51876=CARTESIAN_POINT('Ctrl Pts',(-20.4144844931047,24.2939457223215,24.2290277834884));
#51877=CARTESIAN_POINT('Ctrl Pts',(-20.4140727441406,24.2922074452866,24.2289169359829));
#51878=CARTESIAN_POINT('Ctrl Pts',(-20.4130878261693,24.2880339570874,24.2286510530411));
#51879=CARTESIAN_POINT('Ctrl Pts',(-20.4125160459627,24.2855984145647,24.2284960984256));
#51880=CARTESIAN_POINT('Ctrl Pts',(-20.4104547671604,24.2767720574443,24.227935291115));
#51881=CARTESIAN_POINT('Ctrl Pts',(-20.4089819393871,24.2703773064123,24.2275303972549));
#51882=CARTESIAN_POINT('Ctrl Pts',(-20.3853819170214,24.166460108823,24.220973008481));
#51883=CARTESIAN_POINT('Ctrl Pts',(-20.3677835048837,24.0679525574876,24.215075162204));
#51884=CARTESIAN_POINT('Ctrl Pts',(-20.3359322652538,23.8247654970151,24.2009392795981));
#51885=CARTESIAN_POINT('Ctrl Pts',(-20.3268263135013,23.6796371019528,24.1928604504361));
#51886=CARTESIAN_POINT('Ctrl Pts',(-20.3282805640026,23.3843225230612,24.1763558200481));
#51887=CARTESIAN_POINT('Ctrl Pts',(-20.3394994951309,23.2345045387215,24.1679448463602));
#51888=CARTESIAN_POINT('Ctrl Pts',(-20.3716359015178,23.0137361645292,24.1550303038649));
#51889=CARTESIAN_POINT('Ctrl Pts',(-20.3846122069129,22.9418335279393,24.1507424535152));
#51890=CARTESIAN_POINT('Ctrl Pts',(-20.4092800108476,22.82752401855,24.1437563605225));
#51891=CARTESIAN_POINT('Ctrl Pts',(-20.4194161751385,22.7848060610108,24.1411073069936));
#51892=CARTESIAN_POINT('Ctrl Pts',(-20.4323425579423,22.7348914558426,24.1379625067953));
#51893=CARTESIAN_POINT('Ctrl Pts',(-20.4342901825287,22.7274798258884,24.1374942601693));
#51894=CARTESIAN_POINT('Ctrl Pts',(-20.4373118555928,22.7161455542953,24.1367761956621));
#51895=CARTESIAN_POINT('Ctrl Pts',(-20.4383669346938,22.7122178464856,24.1365269944512));
#51896=CARTESIAN_POINT('Ctrl Pts',(-20.4403029550873,22.705064758111,24.136072478375));
#51897=CARTESIAN_POINT('Ctrl Pts',(-20.4411814876348,22.7018387266974,24.1358672421408));
#51898=CARTESIAN_POINT('Ctrl Pts',(-20.442956521802,22.6953604623846,24.1354545975078));
#51899=CARTESIAN_POINT('Ctrl Pts',(-20.443853112825,22.6921082585257,24.135247186418));
#51900=CARTESIAN_POINT('Ctrl Pts',(-20.4464152554957,22.6828712328369,24.1346573585358));
#51901=CARTESIAN_POINT('Ctrl Pts',(-20.4480930010358,22.6768898348684,24.1342745445432));
#51902=CARTESIAN_POINT('Ctrl Pts',(-20.4552580204885,22.6516266722458,24.1326539587713));
#51903=CARTESIAN_POINT('Ctrl Pts',(-20.4609077596964,22.6323918068861,24.1314108904882));
#51904=CARTESIAN_POINT('Ctrl Pts',(-20.579037814021,22.2436619568108,24.1060981712028));
#51905=CARTESIAN_POINT('Ctrl Pts',(-20.7568533496482,21.8973641530626,24.0794799751109));
#51906=CARTESIAN_POINT('Ctrl Pts',(-21.0580049383886,21.5040922930838,24.0464784186985));
#51907=CARTESIAN_POINT('Ctrl Pts',(-21.1288552356862,21.4207195381369,24.0393274148467));
#51908=CARTESIAN_POINT('Ctrl Pts',(-21.207017762038,21.3376996614197,24.0321765704504));
#51909=CARTESIAN_POINT('Ctrl Pts',(-21.2102277273648,21.3343050356429,24.0318841254644));
#51910=CARTESIAN_POINT('Ctrl Pts',(-21.2153531969917,21.3289082682564,24.0314191321018));
#51911=CARTESIAN_POINT('Ctrl Pts',(-21.2172639058891,21.3269016120452,24.0312462212755));
#51912=CARTESIAN_POINT('Ctrl Pts',(-21.2208977280138,21.3230951575097,24.030918201333));
#51913=CARTESIAN_POINT('Ctrl Pts',(-21.2226203436965,21.321294890035,24.0307630541035));
#51914=CARTESIAN_POINT('Ctrl Pts',(-21.2256323831372,21.3181543738495,24.0304923899652));
#51915=CARTESIAN_POINT('Ctrl Pts',(-21.2269208806809,21.3168132419883,24.0303768005737));
#51916=CARTESIAN_POINT('Ctrl Pts',(-21.229442314416,21.3141933524269,24.0301509900592));
#51917=CARTESIAN_POINT('Ctrl Pts',(-21.2306751439847,21.3129145017412,24.0300407610879));
#51918=CARTESIAN_POINT('Ctrl Pts',(-21.2336206654936,21.3098640763665,24.0297778225378));
#51919=CARTESIAN_POINT('Ctrl Pts',(-21.2353343362327,21.308093442183,24.0296251898184));
#51920=CARTESIAN_POINT('Ctrl Pts',(-21.2405215403746,21.3027460982412,24.029164203487));
#51921=CARTESIAN_POINT('Ctrl Pts',(-21.2440013654985,21.2991754606271,24.0288563394914));
#51922=CARTESIAN_POINT('Ctrl Pts',(-21.2796475405569,21.262768447828,24.0257166485799));
#51923=CARTESIAN_POINT('Ctrl Pts',(-21.3125066541611,21.230613684264,24.0229383125195));
#51924=CARTESIAN_POINT('Ctrl Pts',(-21.3478602393354,21.1974686598157,24.0200539227875));
#51925=CARTESIAN_POINT('Ctrl Pts',(-21.3496779478041,21.1957684569927,24.0199059072776));
#51926=CARTESIAN_POINT('Ctrl Pts',(-21.5687857356509,20.9913002593508,24.00209811902));
#51927=CARTESIAN_POINT('Ctrl Pts',(-21.8131028881281,20.819536931826,23.9861602636745));
#51928=CARTESIAN_POINT('Ctrl Pts',(-22.1683941379893,20.6370035107918,23.9634465376667));
#51929=CARTESIAN_POINT('Ctrl Pts',(-22.2614169239764,20.5946726194036,23.9575507063536));
#51930=CARTESIAN_POINT('Ctrl Pts',(-22.4168138936112,20.5326904840661,23.9476581122768));
#51931=CARTESIAN_POINT('Ctrl Pts',(-22.4780551433208,20.5103914005395,23.9437495198142));
#51932=CARTESIAN_POINT('Ctrl Pts',(-22.547945110198,20.4873178782211,23.9392632779311));
#51933=CARTESIAN_POINT('Ctrl Pts',(-22.5559734687301,20.4847023361426,23.9387475671025));
#51934=CARTESIAN_POINT('Ctrl Pts',(-22.5680386949508,20.4808240129829,23.9379719572683));
#51935=CARTESIAN_POINT('Ctrl Pts',(-22.5720679652259,20.4795375650744,23.9377128388575));
#51936=CARTESIAN_POINT('Ctrl Pts',(-22.5789982108657,20.4773399308067,23.937266989186));
#51937=CARTESIAN_POINT('Ctrl Pts',(-22.5818979718701,20.4764249088786,23.9370803844784));
#51938=CARTESIAN_POINT('Ctrl Pts',(-22.5878689346973,20.4745500544841,23.9366960341396));
#51939=CARTESIAN_POINT('Ctrl Pts',(-22.5909402870981,20.4735907151589,23.9364982725071));
#51940=CARTESIAN_POINT('Ctrl Pts',(-22.5983319461898,20.4712940690194,23.936022185967));
#51941=CARTESIAN_POINT('Ctrl Pts',(-22.6026536328475,20.4699612560899,23.9357437137106));
#51942=CARTESIAN_POINT('Ctrl Pts',(-22.6159064614918,20.4659045992508,23.9348893832668));
#51943=CARTESIAN_POINT('Ctrl Pts',(-22.6248465879802,20.4632104873314,23.9343125510196));
#51944=CARTESIAN_POINT('Ctrl Pts',(-22.6580599892546,20.4533588538683,23.9321675711633));
#51945=CARTESIAN_POINT('Ctrl Pts',(-22.6824051009921,20.4464486134971,23.930591368066));
#51946=CARTESIAN_POINT('Ctrl Pts',(-22.7126467914289,20.4382482695302,23.9286280782575));
#51947=CARTESIAN_POINT('Ctrl Pts',(-22.7184694446759,20.4366869230702,23.9282498293846));
#51948=CARTESIAN_POINT('Ctrl Pts',(-22.7309281087085,20.4333835701199,23.9274399688955));
#51949=CARTESIAN_POINT('Ctrl Pts',(-22.7375653611147,20.4316464014928,23.9270082040032));
#51950=CARTESIAN_POINT('Ctrl Pts',(-22.7458004291177,20.4295191111709,23.9264720982249));
#51951=CARTESIAN_POINT('Ctrl Pts',(-22.7473931014676,20.4291089908439,23.9263683961725));
#51952=CARTESIAN_POINT('Ctrl Pts',(-22.7556086698187,20.4270001493663,23.925833368378));
#51953=CARTESIAN_POINT('Ctrl Pts',(-22.7622366066637,20.4253212985825,23.9254014116947));
#51954=CARTESIAN_POINT('Ctrl Pts',(-22.7723405604248,20.4227961649249,23.9247424207801));
#51955=CARTESIAN_POINT('Ctrl Pts',(-22.7758127563559,20.4219345498868,23.9245158715041));
#51956=CARTESIAN_POINT('Ctrl Pts',(-22.7833158127943,20.4200859460753,23.9240261290462));
#51957=CARTESIAN_POINT('Ctrl Pts',(-22.7873471557163,20.4191009589386,23.9237628735203));
#51958=CARTESIAN_POINT('Ctrl Pts',(-22.7952959548634,20.417175073127,23.9232435615939));
#51959=CARTESIAN_POINT('Ctrl Pts',(-22.799213296126,20.4162337281952,23.9229875196409));
#51960=CARTESIAN_POINT('Ctrl Pts',(-22.8089984399459,20.4139017383293,23.9223476662059));
#51961=CARTESIAN_POINT('Ctrl Pts',(-22.814868382238,20.4125202168652,23.9219635732011));
#51962=CARTESIAN_POINT('Ctrl Pts',(-22.8364318467683,20.4075089764329,23.9205516490563));
#51963=CARTESIAN_POINT('Ctrl Pts',(-22.8521484465184,20.4039805002535,23.9195207298533));
#51964=CARTESIAN_POINT('Ctrl Pts',(-22.8975508445778,20.394144312824,23.9165372789906));
#51965=CARTESIAN_POINT('Ctrl Pts',(-22.927299567814,20.3881380346806,23.9145759066279));
#51966=CARTESIAN_POINT('Ctrl Pts',(-23.2082670368598,20.3355292846434,23.8959911274453));
#51967=CARTESIAN_POINT('Ctrl Pts',(-23.4640869132482,20.3185436469362,23.8785127485977));
#51968=CARTESIAN_POINT('Ctrl Pts',(-23.7879343040884,20.3355416915318,23.8567171755437));
#51969=CARTESIAN_POINT('Ctrl Pts',(-23.8565637541417,20.3413535308889,23.8521242672328));
#51970=CARTESIAN_POINT('Ctrl Pts',(-23.9919860830327,20.3572064253177,23.8431721891027));
#51971=CARTESIAN_POINT('Ctrl Pts',(-24.0587576333294,20.3671571698106,23.8388123171702));
#51972=CARTESIAN_POINT('Ctrl Pts',(-24.1322871931553,20.3804882668886,23.834106666341));
#51973=CARTESIAN_POINT('Ctrl Pts',(-24.1393973572563,20.3818020873211,23.8336526369049));
#51974=CARTESIAN_POINT('Ctrl Pts',(-24.1502194975346,20.3838394974567,23.8329631572826));
#51975=CARTESIAN_POINT('Ctrl Pts',(-24.1539346640711,20.3845456995818,23.8327267481913));
#51976=CARTESIAN_POINT('Ctrl Pts',(-24.1600060322178,20.3857108597834,23.8323408806923));
#51977=CARTESIAN_POINT('Ctrl Pts',(-24.1623629662189,20.3861659114043,23.8321912021973));
#51978=CARTESIAN_POINT('Ctrl Pts',(-24.1668293928583,20.3870334187009,23.8319077840035));
#51979=CARTESIAN_POINT('Ctrl Pts',(-24.1689389837203,20.3874453518819,23.8317740145482));
#51980=CARTESIAN_POINT('Ctrl Pts',(-24.1728438980564,20.3882119086248,23.831526581589));
#51981=CARTESIAN_POINT('Ctrl Pts',(-24.1746393272552,20.3885659499798,23.8314128850436));
#51982=CARTESIAN_POINT('Ctrl Pts',(-24.1782688065368,20.3892848605778,23.8311831879552));
#51983=CARTESIAN_POINT('Ctrl Pts',(-24.1801028336594,20.3896497954321,23.8310671917254));
#51984=CARTESIAN_POINT('Ctrl Pts',(-24.1852901459752,20.3906866616866,23.8307393148959));
#51985=CARTESIAN_POINT('Ctrl Pts',(-24.1886426935298,20.3913623373382,23.8305276498244));
#51986=CARTESIAN_POINT('Ctrl Pts',(-24.2026294356373,20.394204414728,23.8296455704051));
#51987=CARTESIAN_POINT('Ctrl Pts',(-24.2132538888759,20.3964192213056,23.8289779048477));
#51988=CARTESIAN_POINT('Ctrl Pts',(-24.406097133411,20.4376374831104,23.8168989428429));
#51989=CARTESIAN_POINT('Ctrl Pts',(-24.5846366945477,20.4923260876322,23.8063519688607));
#51990=CARTESIAN_POINT('Ctrl Pts',(-24.9130389012636,20.6250033620222,23.7865051127374));
#51991=CARTESIAN_POINT('Ctrl Pts',(-25.0634562250204,20.6999048394407,23.7772124034418));
#51992=CARTESIAN_POINT('Ctrl Pts',(-25.2830197201155,20.8315362892584,23.7625818756211));
#51993=CARTESIAN_POINT('Ctrl Pts',(-25.3567835329952,20.8799821174058,23.7574678848823));
#51994=CARTESIAN_POINT('Ctrl Pts',(-25.4797660129378,20.9681834011257,23.7485105406967));
#51995=CARTESIAN_POINT('Ctrl Pts',(-25.5299733442888,21.0064742525585,23.74472164056));
#51996=CARTESIAN_POINT('Ctrl Pts',(-25.5855362037797,21.0514911904804,23.740362577383));
#51997=CARTESIAN_POINT('Ctrl Pts',(-25.5920303696722,21.056794867235,23.7398504523469));
#51998=CARTESIAN_POINT('Ctrl Pts',(-25.601759934384,21.0648043372006,23.7390791756531));
#51999=CARTESIAN_POINT('Ctrl Pts',(-25.6050108749186,21.0674912661906,23.7388207915778));
#52000=CARTESIAN_POINT('Ctrl Pts',(-25.6105951664282,21.0721252094221,23.7383757817806));
#52001=CARTESIAN_POINT('Ctrl Pts',(-25.6129310608601,21.0740691614432,23.7381892812769));
#52002=CARTESIAN_POINT('Ctrl Pts',(-25.6177380816398,21.0780811285662,23.7378047509909));
#52003=CARTESIAN_POINT('Ctrl Pts',(-25.6202088624547,21.0801495511901,23.7376067046239));
#52004=CARTESIAN_POINT('Ctrl Pts',(-25.6261529768523,21.0851408685647,23.7371292846229));
#52005=CARTESIAN_POINT('Ctrl Pts',(-25.6296232381547,21.0880673975723,23.7368497618239));
#52006=CARTESIAN_POINT('Ctrl Pts',(-25.640265349037,21.0970806116783,23.7359900961001));
#52007=CARTESIAN_POINT('Ctrl Pts',(-25.6474166942058,21.1031913313406,23.7354089624116));
#52008=CARTESIAN_POINT('Ctrl Pts',(-25.7312437946933,21.1754577149339,23.7285559719345));
#52009=CARTESIAN_POINT('Ctrl Pts',(-25.8047791752259,21.245154007265,23.7221359461539));
#52010=CARTESIAN_POINT('Ctrl Pts',(-26.0445149325752,21.4948345416373,23.699715663462));
#52011=CARTESIAN_POINT('Ctrl Pts',(-26.1934186683054,21.6902178902584,23.6830417012337));
#52012=CARTESIAN_POINT('Ctrl Pts',(-26.3564504928827,21.9638110536724,23.6615584173974));
#52013=CARTESIAN_POINT('Ctrl Pts',(-26.3919787330574,22.0283666292493,23.6566172964087));
#52014=CARTESIAN_POINT('Ctrl Pts',(-26.4540121568934,22.1508435559601,23.6475420414925));
#52015=CARTESIAN_POINT('Ctrl Pts',(-26.4810746203063,22.2084446127116,23.6433917371907));
#52016=CARTESIAN_POINT('Ctrl Pts',(-26.5175866582589,22.2925432732204,23.6375371242707));
#52017=CARTESIAN_POINT('Ctrl Pts',(-26.5284216876515,22.3184193418411,23.635763045413));
#52018=CARTESIAN_POINT('Ctrl Pts',(-26.5405756839597,22.3485434827571,23.6337319238414));
#52019=CARTESIAN_POINT('Ctrl Pts',(-26.5422249889197,22.3526557677388,23.6334553859522));
#52020=CARTESIAN_POINT('Ctrl Pts',(-26.5447169420629,22.358906343708,23.6330361818604));
#52021=CARTESIAN_POINT('Ctrl Pts',(-26.545565783641,22.3610421350927,23.632893141357));
#52022=CARTESIAN_POINT('Ctrl Pts',(-26.5470993477564,22.3649128325947,23.6326342725226));
#52023=CARTESIAN_POINT('Ctrl Pts',(-26.5477848468397,22.3666474197936,23.632518397177));
#52024=CARTESIAN_POINT('Ctrl Pts',(-26.5492637708638,22.3703992152115,23.6322680527949));
#52025=CARTESIAN_POINT('Ctrl Pts',(-26.5500566643844,22.3724166234955,23.6321336164919));
#52026=CARTESIAN_POINT('Ctrl Pts',(-26.5522065531198,22.3779029717671,23.6317684973335));
#52027=CARTESIAN_POINT('Ctrl Pts',(-26.5535595758579,22.3813734805415,23.6315380553496));
#52028=CARTESIAN_POINT('Ctrl Pts',(-26.5599541403618,22.3978599677737,23.6304457930726));
#52029=CARTESIAN_POINT('Ctrl Pts',(-26.5649172029267,22.4109065213433,23.6295886497327));
#52030=CARTESIAN_POINT('Ctrl Pts',(-26.6506865970382,22.6408558026825,23.6146009360132));
#52031=CARTESIAN_POINT('Ctrl Pts',(-26.7079927262532,22.8658494421183,23.60177480645));
#52032=CARTESIAN_POINT('Ctrl Pts',(-26.7621191517465,23.245232674654,23.580360255278));
#52033=CARTESIAN_POINT('Ctrl Pts',(-26.7729136765701,23.396710145265,23.5718685391151));
#52034=CARTESIAN_POINT('Ctrl Pts',(-26.7730337244058,23.6028861875044,23.5599467049804));
#52035=CARTESIAN_POINT('Ctrl Pts',(-26.7716824729589,23.6573860561336,23.5567621264744));
#52036=CARTESIAN_POINT('Ctrl Pts',(-26.7684163199079,23.7224519651731,23.5529079856937));
#52037=CARTESIAN_POINT('Ctrl Pts',(-26.7678301562474,23.7330776909892,23.5522769197587));
#52038=CARTESIAN_POINT('Ctrl Pts',(-26.7640140907488,23.7965369586755,23.5484977530617));
#52039=CARTESIAN_POINT('Ctrl Pts',(-26.7595357163768,23.8492848328829,23.5453136282492));
#52040=CARTESIAN_POINT('Ctrl Pts',(-26.7528078681871,23.910576174877,23.5415560497455));
#52041=CARTESIAN_POINT('Ctrl Pts',(-26.7518198229835,23.9192521090897,23.5410228087823));
#52042=CARTESIAN_POINT('Ctrl Pts',(-26.7502940335703,23.9321822837499,23.5402260493789));
#52043=CARTESIAN_POINT('Ctrl Pts',(-26.749783032834,23.9364396899857,23.5399633766331));
#52044=CARTESIAN_POINT('Ctrl Pts',(-26.7488561600969,23.9440338129979,23.5394942408712));
#52045=CARTESIAN_POINT('Ctrl Pts',(-26.7484435590836,23.9473709288078,23.5392878816092));
#52046=CARTESIAN_POINT('Ctrl Pts',(-26.7475623473083,23.9544077155919,23.5388523084232));
#52047=CARTESIAN_POINT('Ctrl Pts',(-26.7470925363722,23.9581072288567,23.5386230567963));
#52048=CARTESIAN_POINT('Ctrl Pts',(-26.7458338894795,23.9678826154407,23.5380166199728));
#52049=CARTESIAN_POINT('Ctrl Pts',(-26.7450341492029,23.9739570474523,23.5376390899753));
#52050=CARTESIAN_POINT('Ctrl Pts',(-26.7413299466234,24.0014855165775,23.5359250187717));
#52051=CARTESIAN_POINT('Ctrl Pts',(-26.7382267197819,24.0229118317863,23.5345821927953));
#52052=CARTESIAN_POINT('Ctrl Pts',(-26.7138403689159,24.1801059625506,23.5246646377594));
#52053=CARTESIAN_POINT('Ctrl Pts',(-26.6841112165263,24.3144018043241,23.5158204466399));
#52054=CARTESIAN_POINT('Ctrl Pts',(-26.5987161015817,24.6093987748373,23.495558382615));
#52055=CARTESIAN_POINT('Ctrl Pts',(-26.5387238363553,24.7684282110944,23.4840491819084));
#52056=CARTESIAN_POINT('Ctrl Pts',(-26.4120338920182,25.0377663994039,23.4639181694639));
#52057=CARTESIAN_POINT('Ctrl Pts',(-26.350719678137,25.1502146047646,23.4553054722273));
#52058=CARTESIAN_POINT('Ctrl Pts',(-26.2807743243951,25.262088982482,23.4467060406426));
#52059=CARTESIAN_POINT('Ctrl Pts',(-26.2786654153686,25.2654482730443,23.4464477975108));
#52060=CARTESIAN_POINT('Ctrl Pts',(-26.2749494112357,25.271343316555,23.4459945872238));
#52061=CARTESIAN_POINT('Ctrl Pts',(-26.2733449685139,25.2738807270362,23.4457995006479));
#52062=CARTESIAN_POINT('Ctrl Pts',(-26.2434950715683,25.3209423387497,23.4421810616369));
#52063=CARTESIAN_POINT('Ctrl Pts',(-26.2141625571307,25.3647722906092,23.4388085414191));
#52064=CARTESIAN_POINT('Ctrl Pts',(-26.1804541774281,25.412560204773,23.4351458251695));
#52065=CARTESIAN_POINT('Ctrl Pts',(-26.1771302012833,25.4172459105409,23.4347868452795));
#52066=CARTESIAN_POINT('Ctrl Pts',(-26.1724575334191,25.4237956415432,23.4342853088049));
#52067=CARTESIAN_POINT('Ctrl Pts',(-26.1711193736686,25.4256671131279,23.4341420321235));
#52068=CARTESIAN_POINT('Ctrl Pts',(-26.1686677119342,25.429088114516,23.4338801809408));
#52069=CARTESIAN_POINT('Ctrl Pts',(-26.1675548363527,25.4306380904229,23.4337615629291));
#52070=CARTESIAN_POINT('Ctrl Pts',(-26.1652920937829,25.4337836621232,23.4335208791497));
#52071=CARTESIAN_POINT('Ctrl Pts',(-26.1641421423972,25.4353791942007,23.4333988195092));
#52072=CARTESIAN_POINT('Ctrl Pts',(-26.161281865988,25.4393401152093,23.4330958591404));
#52073=CARTESIAN_POINT('Ctrl Pts',(-26.1595697821979,25.4417042411277,23.4329150810102));
#52074=CARTESIAN_POINT('Ctrl Pts',(-26.1531645303461,25.4505236666209,23.4322408486565));
#52075=CARTESIAN_POINT('Ctrl Pts',(-26.1484505492332,25.4569639214481,23.431748830262));
#52076=CARTESIAN_POINT('Ctrl Pts',(-26.0676479113083,25.5665006300306,23.423384906643));
#52077=CARTESIAN_POINT('Ctrl Pts',(-25.9854905246638,25.6650008999539,23.415928755296));
#52078=CARTESIAN_POINT('Ctrl Pts',(-25.7809629251301,25.8824328170575,23.3989388119674));
#52079=CARTESIAN_POINT('Ctrl Pts',(-25.6545953285815,25.9970624735601,23.3895461567267));
#52080=CARTESIAN_POINT('Ctrl Pts',(-25.3587610343776,26.2254692212081,23.3685210633742));
#52081=CARTESIAN_POINT('Ctrl Pts',(-25.1863876927914,26.3342299611382,23.3568378700138));
#52082=CARTESIAN_POINT('Ctrl Pts',(-24.9930187205028,26.4320439080216,23.3436762714391));
#52083=CARTESIAN_POINT('Ctrl Pts',(-24.9810679790176,26.4379961074888,23.3428628169562));
#52084=CARTESIAN_POINT('Ctrl Pts',(-24.9648306322879,26.4459577594516,23.3417574249243));
#52085=CARTESIAN_POINT('Ctrl Pts',(-24.9605759600465,26.4480323362677,23.3414677643208));
#52086=CARTESIAN_POINT('Ctrl Pts',(-24.9533693527638,26.4515266446439,23.3409771033074));
#52087=CARTESIAN_POINT('Ctrl Pts',(-24.9504197860793,26.4529512676414,23.340776273665));
#52088=CARTESIAN_POINT('Ctrl Pts',(-24.9447437487876,26.4556820950769,23.3403897855184));
#52089=CARTESIAN_POINT('Ctrl Pts',(-24.942017601317,26.4569889650862,23.3402041504798));
#52090=CARTESIAN_POINT('Ctrl Pts',(-24.9356691372612,26.4600213352388,23.3397718348371));
#52091=CARTESIAN_POINT('Ctrl Pts',(-24.9320454350061,26.4617439078086,23.3395250528141));
#52092=CARTESIAN_POINT('Ctrl Pts',(-24.9216296197132,26.4666713715025,23.3388156606069));
#52093=CARTESIAN_POINT('Ctrl Pts',(-24.9148295417498,26.4698592772731,23.338352462181));
#52094=CARTESIAN_POINT('Ctrl Pts',(-24.8995137383653,26.4769741955195,23.3373090302286));
#52095=CARTESIAN_POINT('Ctrl Pts',(-24.8909919178829,26.4808878547364,23.3367283389426));
#52096=CARTESIAN_POINT('Ctrl Pts',(-24.8210116240697,26.5126572952353,23.3319586195421));
#52097=CARTESIAN_POINT('Ctrl Pts',(-24.758713284732,26.538611973336,23.3277047335592));
#52098=CARTESIAN_POINT('Ctrl Pts',(-24.579411373383,26.6067888874818,23.3154279353687));
#52099=CARTESIAN_POINT('Ctrl Pts',(-24.4607245844803,26.6442171624869,23.3072573148523));
#52100=CARTESIAN_POINT('Ctrl Pts',(-24.049573260902,26.7481657449141,23.2789171562144));
#52101=CARTESIAN_POINT('Ctrl Pts',(-23.7501395105374,26.7807356974758,23.258080567559));
#52102=CARTESIAN_POINT('Ctrl Pts',(-23.4344913771458,26.7709627075555,23.2380978145809));
#52103=CARTESIAN_POINT('Ctrl Pts',(-23.4184676449365,26.7703468549784,23.2370892152386));
#52104=CARTESIAN_POINT('Ctrl Pts',(-23.3988804525591,26.7694475888472,23.2358639784014));
#52105=CARTESIAN_POINT('Ctrl Pts',(-23.3953123729465,26.7692778298011,23.2356410954923));
#52106=CARTESIAN_POINT('Ctrl Pts',(-23.3894265749547,26.7689879915044,23.2352739558622));
#52107=CARTESIAN_POINT('Ctrl Pts',(-23.3871087037833,26.7688713410729,23.235129506952));
#52108=CARTESIAN_POINT('Ctrl Pts',(-23.3829268239884,26.7686563525653,23.2348691368994));
#52109=CARTESIAN_POINT('Ctrl Pts',(-23.3810627794657,26.7685588990956,23.2347531660722));
#52110=CARTESIAN_POINT('Ctrl Pts',(-23.3770513672059,26.7683456850442,23.2345037859032));
#52111=CARTESIAN_POINT('Ctrl Pts',(-23.3749040363296,26.7682293949201,23.234370407178));
#52112=CARTESIAN_POINT('Ctrl Pts',(-23.369015418782,26.7679045812555,23.2340049569704));
#52113=CARTESIAN_POINT('Ctrl Pts',(-23.3652743618624,26.7676916811059,23.2337731327197));
#52114=CARTESIAN_POINT('Ctrl Pts',(-23.3457357164493,26.7665455638401,23.2325641452823));
#52115=CARTESIAN_POINT('Ctrl Pts',(-23.3299444289777,26.765502500269,23.2315930943731));
#52116=CARTESIAN_POINT('Ctrl Pts',(-23.1721618368714,26.7539125593274,23.2219455239268));
#52117=CARTESIAN_POINT('Ctrl Pts',(-23.0309897994891,26.7340815556433,23.2137557014296));
#52118=CARTESIAN_POINT('Ctrl Pts',(-22.6073671109249,26.6456330650418,23.189312105101));
#52119=CARTESIAN_POINT('Ctrl Pts',(-22.3327375190274,26.5482166443642,23.1735174004987));
#52120=CARTESIAN_POINT('Ctrl Pts',(-22.0750359362473,26.4155367338316,23.1563971075561));
#52121=CARTESIAN_POINT('',(-26.7730015390511,23.5527819743835,23.3126472226381));
#52122=CARTESIAN_POINT('Ctrl Pts',(-22.0750361284943,26.4155368328116,22.9065074728514));
#52123=CARTESIAN_POINT('Ctrl Pts',(-22.16486243135,26.4617846817109,22.9121756008112));
#52124=CARTESIAN_POINT('Ctrl Pts',(-22.2568402343458,26.503796477144,22.9178886654819));
#52125=CARTESIAN_POINT('Ctrl Pts',(-22.4634598636861,26.5866595062593,22.930728433918));
#52126=CARTESIAN_POINT('Ctrl Pts',(-22.5787072220492,26.6254728442691,22.9378960149764));
#52127=CARTESIAN_POINT('Ctrl Pts',(-22.7061805969438,26.6605217590922,22.9459399633442));
#52128=CARTESIAN_POINT('Ctrl Pts',(-22.7165137408078,26.6633075781343,22.94659278619));
#52129=CARTESIAN_POINT('Ctrl Pts',(-22.731026096484,26.6671426764694,22.9475107827341));
#52130=CARTESIAN_POINT('Ctrl Pts',(-22.7351939080936,26.668235143343,22.9477745543495));
#52131=CARTESIAN_POINT('Ctrl Pts',(-22.7424234913705,26.6701146757686,22.9482323315499));
#52132=CARTESIAN_POINT('Ctrl Pts',(-22.7454842612207,26.670905602311,22.9484262117402));
#52133=CARTESIAN_POINT('Ctrl Pts',(-22.7518487756404,26.6725402556949,22.9488295152566));
#52134=CARTESIAN_POINT('Ctrl Pts',(-22.755152703572,26.673383244986,22.9490389621639));
#52135=CARTESIAN_POINT('Ctrl Pts',(-22.7617100578641,26.6750452584321,22.9494548258914));
#52136=CARTESIAN_POINT('Ctrl Pts',(-22.7649634377647,26.6758644488918,22.9496612370104));
#52137=CARTESIAN_POINT('Ctrl Pts',(-22.7758569297536,26.6785893129885,22.9503526595473));
#52138=CARTESIAN_POINT('Ctrl Pts',(-22.7835027006515,26.6804720544012,22.9508384119548));
#52139=CARTESIAN_POINT('Ctrl Pts',(-22.8397413044736,26.6941021822103,22.9544148994032));
#52140=CARTESIAN_POINT('Ctrl Pts',(-22.8885924204813,26.7047449270611,22.9575410713065));
#52141=CARTESIAN_POINT('Ctrl Pts',(-23.0486486025913,26.7357335275974,22.9678547127887));
#52142=CARTESIAN_POINT('Ctrl Pts',(-23.160669796055,26.7513642361478,22.9751874512787));
#52143=CARTESIAN_POINT('Ctrl Pts',(-23.3562780135944,26.7682383857494,22.9881710696797));
#52144=CARTESIAN_POINT('Ctrl Pts',(-23.439527952971,26.7721770962261,22.993751550224));
#52145=CARTESIAN_POINT('Ctrl Pts',(-23.7778558200211,26.7750557104828,23.0165633111645));
#52146=CARTESIAN_POINT('Ctrl Pts',(-24.0322509006624,26.7469471236772,23.0340964832569));
#52147=CARTESIAN_POINT('Ctrl Pts',(-24.2840444306947,26.6883536956621,23.0504393210503));
#52148=CARTESIAN_POINT('Ctrl Pts',(-24.2874035980655,26.6875663145234,23.0506571495124));
#52149=CARTESIAN_POINT('Ctrl Pts',(-24.3024872406425,26.6840051801437,23.0516343411892));
#52150=CARTESIAN_POINT('Ctrl Pts',(-24.3141975750192,26.6811710392117,23.0523904906597));
#52151=CARTESIAN_POINT('Ctrl Pts',(-24.3293505191172,26.677413638132,23.0533654389536));
#52152=CARTESIAN_POINT('Ctrl Pts',(-24.3328076750557,26.6765502954261,23.0535876379502));
#52153=CARTESIAN_POINT('Ctrl Pts',(-24.3381050207881,26.6752180713369,23.0539277401309));
#52154=CARTESIAN_POINT('Ctrl Pts',(-24.339946225556,26.6747532979678,23.0540458813019));
#52155=CARTESIAN_POINT('Ctrl Pts',(-24.3435767155369,26.6738334431553,23.0542786955077));
#52156=CARTESIAN_POINT('Ctrl Pts',(-24.3453660111084,26.6733784539079,23.0543933727857));
#52157=CARTESIAN_POINT('Ctrl Pts',(-24.3493515075746,26.6723613588228,23.054648660191));
#52158=CARTESIAN_POINT('Ctrl Pts',(-24.3515475015713,26.6717984744945,23.0547892240513));
#52159=CARTESIAN_POINT('Ctrl Pts',(-24.3578898036611,26.6701656612485,23.0551949098688));
#52160=CARTESIAN_POINT('Ctrl Pts',(-24.3620345959232,26.66908977973,23.0554596859208));
#52161=CARTESIAN_POINT('Ctrl Pts',(-24.3900264793534,26.6617642253519,23.0572455908411));
#52162=CARTESIAN_POINT('Ctrl Pts',(-24.413804170551,26.6552491434057,23.0587515262944));
#52163=CARTESIAN_POINT('Ctrl Pts',(-24.4871265250587,26.6342513722177,23.0633675489862));
#52164=CARTESIAN_POINT('Ctrl Pts',(-24.5364019439207,26.6188502101736,23.066430245394));
#52165=CARTESIAN_POINT('Ctrl Pts',(-24.7188282838925,26.5569836408599,23.0776938290128));
#52166=CARTESIAN_POINT('Ctrl Pts',(-24.8492622942659,26.5029768943138,23.0856005256094));
#52167=CARTESIAN_POINT('Ctrl Pts',(-25.0331190976727,26.4123001257836,23.0970622360891));
#52168=CARTESIAN_POINT('Ctrl Pts',(-25.0896353729596,26.382303043671,23.1006308854553));
#52169=CARTESIAN_POINT('Ctrl Pts',(-25.2166588277112,26.3099565791244,23.1088236462832));
#52170=CARTESIAN_POINT('Ctrl Pts',(-25.2865111857637,26.2665517522373,23.1134558703007));
#52171=CARTESIAN_POINT('Ctrl Pts',(-25.4073953590702,26.1848671586225,23.1217943080966));
#52172=CARTESIAN_POINT('Ctrl Pts',(-25.4590943008135,26.147654342409,23.1254719169986));
#52173=CARTESIAN_POINT('Ctrl Pts',(-25.526167127659,26.0962909478847,23.1304189774858));
#52174=CARTESIAN_POINT('Ctrl Pts',(-25.5425562905233,26.0834867910561,23.1316422022653));
#52175=CARTESIAN_POINT('Ctrl Pts',(-25.6098745947229,26.0298364970527,23.1367289408539));
#52176=CARTESIAN_POINT('Ctrl Pts',(-25.6596778609204,25.9876083818812,23.1406422195937));
#52177=CARTESIAN_POINT('Ctrl Pts',(-25.71437272165,25.938300121158,23.1451280259904));
#52178=CARTESIAN_POINT('Ctrl Pts',(-25.7205616286409,25.9326769077774,23.1456384140811));
#52179=CARTESIAN_POINT('Ctrl Pts',(-25.7298832660995,25.9241408445732,23.146411437476));
#52180=CARTESIAN_POINT('Ctrl Pts',(-25.7330322302026,25.9212457092213,23.1466733187197));
#52181=CARTESIAN_POINT('Ctrl Pts',(-25.7384925288226,25.9162054520383,23.1471287204361));
#52182=CARTESIAN_POINT('Ctrl Pts',(-25.7408065019421,25.914063186049,23.1473221186728));
#52183=CARTESIAN_POINT('Ctrl Pts',(-25.7456202204641,25.9095935284785,23.1477252937206));
#52184=CARTESIAN_POINT('Ctrl Pts',(-25.7481194162172,25.9072655536732,23.147935095414));
#52185=CARTESIAN_POINT('Ctrl Pts',(-25.7530736494305,25.9026360060083,23.1483519495873));
#52186=CARTESIAN_POINT('Ctrl Pts',(-25.7555287921281,25.9003345519652,23.1485589968027));
#52187=CARTESIAN_POINT('Ctrl Pts',(-25.7612413370506,25.8949627702342,23.1490418446381));
#52188=CARTESIAN_POINT('Ctrl Pts',(-25.7644959501454,25.8918894983581,23.1493177723483));
#52189=CARTESIAN_POINT('Ctrl Pts',(-25.7829183069544,25.8744208530877,23.1508843851844));
#52190=CARTESIAN_POINT('Ctrl Pts',(-25.7979517762224,25.8598851698296,23.1521811543268));
#52191=CARTESIAN_POINT('Ctrl Pts',(-25.8859572903002,25.7731206569214,23.1598831617822));
#52192=CARTESIAN_POINT('Ctrl Pts',(-25.9555781207076,25.6975914440227,23.1664351755683));
#52193=CARTESIAN_POINT('Ctrl Pts',(-26.0645119790878,25.5674568890809,23.1774925544216));
#52194=CARTESIAN_POINT('Ctrl Pts',(-26.1059360892757,25.5147103901443,23.1819162875233));
#52195=CARTESIAN_POINT('Ctrl Pts',(-26.3313749991614,25.2084433406552,23.2072436915733));
#52196=CARTESIAN_POINT('Ctrl Pts',(-26.4792894316959,24.9304628184962,23.2290824280089));
#52197=CARTESIAN_POINT('Ctrl Pts',(-26.5895313036946,24.6222141476893,23.2497945203404));
#52198=CARTESIAN_POINT('Ctrl Pts',(-26.5942014665338,24.6088799730136,23.2506836771023));
#52199=CARTESIAN_POINT('Ctrl Pts',(-26.6004108189609,24.5907702618418,23.2518816654788));
#52200=CARTESIAN_POINT('Ctrl Pts',(-26.6020266793993,24.5860214616891,23.2521949144694));
#52201=CARTESIAN_POINT('Ctrl Pts',(-26.6044048770155,24.5789783739944,23.2526581616786));
#52202=CARTESIAN_POINT('Ctrl Pts',(-26.6051757207206,24.5766869992998,23.2528086628511));
#52203=CARTESIAN_POINT('Ctrl Pts',(-26.6065402190788,24.5726158010817,23.2530756898644));
#52204=CARTESIAN_POINT('Ctrl Pts',(-26.6071348975369,24.5708363274313,23.2531922767807));
#52205=CARTESIAN_POINT('Ctrl Pts',(-26.6083884109482,24.5670744779233,23.2534384741102));
#52206=CARTESIAN_POINT('Ctrl Pts',(-26.6090468708566,24.5650919855395,23.2535680618269));
#52207=CARTESIAN_POINT('Ctrl Pts',(-26.6107943509794,24.5598135176032,23.2539126772276));
#52208=CARTESIAN_POINT('Ctrl Pts',(-26.6118799783023,24.5565164087705,23.254127502904));
#52209=CARTESIAN_POINT('Ctrl Pts',(-26.6168965153639,24.5411976420071,23.2551236286644));
#52210=CARTESIAN_POINT('Ctrl Pts',(-26.6207620311532,24.5291544473418,23.2559010967138));
#52211=CARTESIAN_POINT('Ctrl Pts',(-26.7131163522605,24.2354901084055,23.2747287003191));
#52212=CARTESIAN_POINT('Ctrl Pts',(-26.7625838218202,23.9430043432626,23.2906579280122));
#52213=CARTESIAN_POINT('Ctrl Pts',(-26.7724844617027,23.6161547217701,23.3090613006868));
#52214=CARTESIAN_POINT('Ctrl Pts',(-26.7729766687258,23.5844691188605,23.3108502788934));
#52215=CARTESIAN_POINT('Ctrl Pts',(-26.7730015390511,23.5527819743835,23.3126472226381));
#52216=CARTESIAN_POINT('Ctrl Pts',(-26.7730015419314,23.5527783018455,23.3126474309038));
#52217=CARTESIAN_POINT('Ctrl Pts',(-26.7731347774501,23.3827768328784,23.3222880338827));
#52218=CARTESIAN_POINT('Ctrl Pts',(-26.7598169813681,23.2130497545595,23.332159750487));
#52219=CARTESIAN_POINT('Ctrl Pts',(-26.7317837701308,23.0363890775716,23.3430267767076));
#52220=CARTESIAN_POINT('Ctrl Pts',(-26.7303534844098,23.0276105905061,23.3435682729724));
#52221=CARTESIAN_POINT('Ctrl Pts',(-26.7280309523797,23.0137184544939,23.3444276207531));
#52222=CARTESIAN_POINT('Ctrl Pts',(-26.7271626518509,23.0086008032555,23.3447447119607));
#52223=CARTESIAN_POINT('Ctrl Pts',(-26.7256636102518,22.9998932583048,23.34528512884));
#52224=CARTESIAN_POINT('Ctrl Pts',(-26.7250391341262,22.9963022844,23.3455082549574));
#52225=CARTESIAN_POINT('Ctrl Pts',(-26.7238659845492,22.9896233755115,23.3459237362949));
#52226=CARTESIAN_POINT('Ctrl Pts',(-26.723318892227,22.9865351641692,23.3461160409375));
#52227=CARTESIAN_POINT('Ctrl Pts',(-26.7221753701466,22.9801346522211,23.3465150072844));
#52228=CARTESIAN_POINT('Ctrl Pts',(-26.7215782582394,22.9768224787617,23.3467216905264));
#52229=CARTESIAN_POINT('Ctrl Pts',(-26.7202043038506,22.9692689542262,23.3471935522447));
#52230=CARTESIAN_POINT('Ctrl Pts',(-26.7194241365904,22.9650282212664,23.3474588365537));
#52231=CARTESIAN_POINT('Ctrl Pts',(-26.717070682939,22.95237834043,23.3482512761457));
#52232=CARTESIAN_POINT('Ctrl Pts',(-26.7154724298395,22.9439739276224,23.3487792282389));
#52233=CARTESIAN_POINT('Ctrl Pts',(-26.7085800061031,22.9085003234153,23.3510138951074));
#52234=CARTESIAN_POINT('Ctrl Pts',(-26.7029720296144,22.8814939627236,23.352730622724));
#52235=CARTESIAN_POINT('Ctrl Pts',(-26.6956565670161,22.848404395219,23.3548536603124));
#52236=CARTESIAN_POINT('Ctrl Pts',(-26.6942768204619,22.842249266999,23.355249412015));
#52237=CARTESIAN_POINT('Ctrl Pts',(-26.6914492003773,22.829806361898,23.3560511463732));
#52238=CARTESIAN_POINT('Ctrl Pts',(-26.6900004967742,22.8235188048581,23.3564571538825));
#52239=CARTESIAN_POINT('Ctrl Pts',(-26.6874628508522,22.812654328269,23.3571602389735));
#52240=CARTESIAN_POINT('Ctrl Pts',(-26.6863827463318,22.8080753474668,23.3574570348753));
#52241=CARTESIAN_POINT('Ctrl Pts',(-26.6821369703648,22.7902506259615,23.3586142215895));
#52242=CARTESIAN_POINT('Ctrl Pts',(-26.6788974116509,22.7770227857997,23.3594769418447));
#52243=CARTESIAN_POINT('Ctrl Pts',(-26.673552638265,22.7557825001647,23.3608686612183));
#52244=CARTESIAN_POINT('Ctrl Pts',(-26.6715001768699,22.7477568481155,23.3613960038698));
#52245=CARTESIAN_POINT('Ctrl Pts',(-26.6653133948758,22.7239477508347,23.3629648445309));
#52246=CARTESIAN_POINT('Ctrl Pts',(-26.6610901767673,22.7081878650457,23.3640090746905));
#52247=CARTESIAN_POINT('Ctrl Pts',(-26.6486937537505,22.6632941787523,23.3670002166191));
#52248=CARTESIAN_POINT('Ctrl Pts',(-26.6402298238597,22.6342430519495,23.3689558027433));
#52249=CARTESIAN_POINT('Ctrl Pts',(-26.6171216119529,22.5588952877054,23.3740797923215));
#52250=CARTESIAN_POINT('Ctrl Pts',(-26.6018382137583,22.5128039213031,23.3772658662748));
#52251=CARTESIAN_POINT('Ctrl Pts',(-26.5788097365262,22.4482736689212,23.3817971389169));
#52252=CARTESIAN_POINT('Ctrl Pts',(-26.5719250045436,22.4295332969381,23.3831215828238));
#52253=CARTESIAN_POINT('Ctrl Pts',(-26.505686457019,22.2542790569056,23.3955853758218));
#52254=CARTESIAN_POINT('Ctrl Pts',(-26.4343989368746,22.1025539560604,23.4069810383859));
#52255=CARTESIAN_POINT('Ctrl Pts',(-26.2715837909986,21.8162660860202,23.4291944643353));
#52256=CARTESIAN_POINT('Ctrl Pts',(-26.1809985326333,21.6816853966507,23.4399837514184));
#52257=CARTESIAN_POINT('Ctrl Pts',(-26.076854025858,21.5496425501844,23.4505216025554));
#52258=CARTESIAN_POINT('Ctrl Pts',(-26.0730304233628,21.544823121512,23.4509061385287));
#52259=CARTESIAN_POINT('Ctrl Pts',(-26.067553470687,21.5379601936359,23.4514535650238));
#52260=CARTESIAN_POINT('Ctrl Pts',(-26.0659114148823,21.5359077611007,23.4516172586076));
#52261=CARTESIAN_POINT('Ctrl Pts',(-26.0630725444527,21.5323682957789,23.4518995134574));
#52262=CARTESIAN_POINT('Ctrl Pts',(-26.0618769180231,21.5308803153493,23.4520181607812));
#52263=CARTESIAN_POINT('Ctrl Pts',(-26.0595758186541,21.5280217573925,23.4522460701185));
#52264=CARTESIAN_POINT('Ctrl Pts',(-26.0584705465304,21.5266510261847,23.4523553463859));
#52265=CARTESIAN_POINT('Ctrl Pts',(-26.0558532241869,21.523410526361,23.4526136598583));
#52266=CARTESIAN_POINT('Ctrl Pts',(-26.0543402010283,21.5215415396651,23.4527626263555));
#52267=CARTESIAN_POINT('Ctrl Pts',(-26.0498323169783,21.5159858283025,23.4532053932629));
#52268=CARTESIAN_POINT('Ctrl Pts',(-26.0468313790559,21.5123040085176,23.4534987560811));
#52269=CARTESIAN_POINT('Ctrl Pts',(-26.0193306965118,21.4787156104459,23.4561746041087));
#52270=CARTESIAN_POINT('Ctrl Pts',(-25.9943014801422,21.4492439016129,23.4585193456803));
#52271=CARTESIAN_POINT('Ctrl Pts',(-25.7888925638333,21.2160164049705,23.4771158766059));
#52272=CARTESIAN_POINT('Ctrl Pts',(-25.58387347536,21.035377384812,23.4918497832071));
#52273=CARTESIAN_POINT('Ctrl Pts',(-25.2848088565358,20.832648678494,23.5122093894683));
#52274=CARTESIAN_POINT('Ctrl Pts',(-25.2090189625916,20.7857364989744,23.5172777257283));
#52275=CARTESIAN_POINT('Ctrl Pts',(-25.0786805971855,20.7123512445099,23.5259442326767));
#52276=CARTESIAN_POINT('Ctrl Pts',(-25.0251525071944,20.6841671377927,23.5294897792611));
#52277=CARTESIAN_POINT('Ctrl Pts',(-24.9228930822792,20.6339480478768,23.5362636539576));
#52278=CARTESIAN_POINT('Ctrl Pts',(-24.8743445586016,20.6115872374527,23.5394797628008));
#52279=CARTESIAN_POINT('Ctrl Pts',(-24.8178844524073,20.5872656181398,23.5432279750036));
#52280=CARTESIAN_POINT('Ctrl Pts',(-24.8104924927464,20.5841140698167,23.5437188552156));
#52281=CARTESIAN_POINT('Ctrl Pts',(-24.799989186852,20.579682355138,23.5444165909233));
#52282=CARTESIAN_POINT('Ctrl Pts',(-24.7968874611815,20.578379345716,23.544622668393));
#52283=CARTESIAN_POINT('Ctrl Pts',(-24.7906331856786,20.5757634902144,23.5450382620369));
#52284=CARTESIAN_POINT('Ctrl Pts',(-24.7874805784183,20.5744507935207,23.5452477829605));
#52285=CARTESIAN_POINT('Ctrl Pts',(-24.781412261389,20.5719353507241,23.5456511440275));
#52286=CARTESIAN_POINT('Ctrl Pts',(-24.7784968591937,20.5707318685117,23.545844958891));
#52287=CARTESIAN_POINT('Ctrl Pts',(-24.7716209536145,20.5679052915997,23.5463021349591));
#52288=CARTESIAN_POINT('Ctrl Pts',(-24.7676589808756,20.5662858060453,23.5465656182724));
#52289=CARTESIAN_POINT('Ctrl Pts',(-24.755937820288,20.5615219249464,23.5473452760056));
#52290=CARTESIAN_POINT('Ctrl Pts',(-24.7481696373871,20.55839988482,23.547862206157));
#52291=CARTESIAN_POINT('Ctrl Pts',(-24.6794642475673,20.5310976013259,23.5524361974753));
#52292=CARTESIAN_POINT('Ctrl Pts',(-24.6178184471994,20.5087532980522,23.5565547133044));
#52293=CARTESIAN_POINT('Ctrl Pts',(-24.4944530175027,20.4682504971379,23.5648340144744));
#52294=CARTESIAN_POINT('Ctrl Pts',(-24.4327855324364,20.4500290390643,23.5689905725245));
#52295=CARTESIAN_POINT('Ctrl Pts',(-24.341211121178,20.4259243273271,23.5751872207995));
#52296=CARTESIAN_POINT('Ctrl Pts',(-24.3116972498808,20.4186005590658,23.5771879417176));
#52297=CARTESIAN_POINT('Ctrl Pts',(-24.1269003131287,20.3755105755429,23.5897339345976));
#52298=CARTESIAN_POINT('Ctrl Pts',(-23.9692549817492,20.3508870366001,23.6005343974073));
#52299=CARTESIAN_POINT('Ctrl Pts',(-23.7902861271128,20.3363902738309,23.612681391724));
#52300=CARTESIAN_POINT('Ctrl Pts',(-23.7701090261057,20.3349469679697,23.6140489804413));
#52301=CARTESIAN_POINT('Ctrl Pts',(-23.7259120492649,20.3322034519652,23.6170391689943));
#52302=CARTESIAN_POINT('Ctrl Pts',(-23.7018883572936,20.3309820021721,23.6186609989363));
#52303=CARTESIAN_POINT('Ctrl Pts',(-23.5933689287527,20.3266819474953,23.6259662012804));
#52304=CARTESIAN_POINT('Ctrl Pts',(-23.5087801657619,20.3266600955778,23.6316041235454));
#52305=CARTESIAN_POINT('Ctrl Pts',(-23.3860665938423,20.3314603176345,23.6396202134002));
#52306=CARTESIAN_POINT('Ctrl Pts',(-23.3478773246794,20.3336355363346,23.6420917550492));
#52307=CARTESIAN_POINT('Ctrl Pts',(-23.2833826691573,20.3384623261021,23.6462167992901));
#52308=CARTESIAN_POINT('Ctrl Pts',(-23.2570554628451,20.3407585781832,23.6478868361096));
#52309=CARTESIAN_POINT('Ctrl Pts',(-23.2264173098206,20.3438109925084,23.6498118728137));
#52310=CARTESIAN_POINT('Ctrl Pts',(-23.2220770116411,20.3442523096551,23.6500841472256));
#52311=CARTESIAN_POINT('Ctrl Pts',(-23.2154657382807,20.344938103699,23.6504982110415));
#52312=CARTESIAN_POINT('Ctrl Pts',(-23.2131941266648,20.3451761814281,23.6506403609315));
#52313=CARTESIAN_POINT('Ctrl Pts',(-23.2090686415916,20.3456129900398,23.6508982977542));
#52314=CARTESIAN_POINT('Ctrl Pts',(-23.2072146938266,20.3458109140884,23.6510141299973));
#52315=CARTESIAN_POINT('Ctrl Pts',(-23.2031940589487,20.3462436789276,23.651265156621));
#52316=CARTESIAN_POINT('Ctrl Pts',(-23.201027443981,20.3464791080123,23.6514003168471));
#52317=CARTESIAN_POINT('Ctrl Pts',(-23.195108462519,20.3471283530118,23.6517692609623));
#52318=CARTESIAN_POINT('Ctrl Pts',(-23.1913565666232,20.3475465663374,23.6520027954816));
#52319=CARTESIAN_POINT('Ctrl Pts',(-23.1732309428666,20.3495992298281,23.653129456525));
#52320=CARTESIAN_POINT('Ctrl Pts',(-23.1588672995124,20.3513238898273,23.6540175443053));
#52321=CARTESIAN_POINT('Ctrl Pts',(-22.8989446196282,20.3843100435371,23.6700103538845));
#52322=CARTESIAN_POINT('Ctrl Pts',(-22.657736849038,20.4436703441888,23.6836305656529));
#52323=CARTESIAN_POINT('Ctrl Pts',(-22.3252827499329,20.5674614776992,23.703470536442));
#52324=CARTESIAN_POINT('Ctrl Pts',(-22.2268208200252,20.6098239239812,23.7094847320403));
#52325=CARTESIAN_POINT('Ctrl Pts',(-22.0405370583965,20.7012258394838,23.7213625775057));
#52326=CARTESIAN_POINT('Ctrl Pts',(-21.9525416825125,20.7496256008681,23.7272050633022));
#52327=CARTESIAN_POINT('Ctrl Pts',(-21.8268398293974,20.8266191141364,23.7359972331346));
#52328=CARTESIAN_POINT('Ctrl Pts',(-21.7872707908356,20.8520632569423,23.7388330501406));
#52329=CARTESIAN_POINT('Ctrl Pts',(-21.7418213928554,20.8827152857721,23.7421760966142));
#52330=CARTESIAN_POINT('Ctrl Pts',(-21.7353843126754,20.8870905974095,23.7426516202695));
#52331=CARTESIAN_POINT('Ctrl Pts',(-21.7262098007181,20.8933752638041,23.7433323131262));
#52332=CARTESIAN_POINT('Ctrl Pts',(-21.7234593515955,20.8952656432011,23.7435367599973));
#52333=CARTESIAN_POINT('Ctrl Pts',(-21.7179126052756,20.8990906131201,23.7439498328076));
#52334=CARTESIAN_POINT('Ctrl Pts',(-21.715116423812,20.9010253632829,23.7441584646665));
#52335=CARTESIAN_POINT('Ctrl Pts',(-21.7097144998507,20.9047757500363,23.7445622899962));
#52336=CARTESIAN_POINT('Ctrl Pts',(-21.7071083677678,20.9065908211465,23.7447574616739));
#52337=CARTESIAN_POINT('Ctrl Pts',(-21.7009267472671,20.9109096667752,23.7452212292737));
#52338=CARTESIAN_POINT('Ctrl Pts',(-21.6973536606085,20.9134168544508,23.745489955989));
#52339=CARTESIAN_POINT('Ctrl Pts',(-21.6847686440322,20.9222858054068,23.7464387997708));
#52340=CARTESIAN_POINT('Ctrl Pts',(-21.6757843732346,20.9286865173327,23.7471204148647));
#52341=CARTESIAN_POINT('Ctrl Pts',(-21.5535299786202,21.0167346154464,23.756454298491));
#52342=CARTESIAN_POINT('Ctrl Pts',(-21.4456657828931,21.1056014229899,23.7653911747509));
#52343=CARTESIAN_POINT('Ctrl Pts',(-21.1534028885981,21.3801047661281,23.791746768356));
#52344=CARTESIAN_POINT('Ctrl Pts',(-20.9853920717037,21.5815229763983,23.8097444451733));
#52345=CARTESIAN_POINT('Ctrl Pts',(-20.818013299452,21.840515637433,23.8302651934157));
#52346=CARTESIAN_POINT('Ctrl Pts',(-20.7933415156972,21.8805898388672,23.8333709171742));
#52347=CARTESIAN_POINT('Ctrl Pts',(-20.7483236270243,21.9574323460465,23.839177392827));
#52348=CARTESIAN_POINT('Ctrl Pts',(-20.7278014726324,21.9940866891688,23.8418852827158));
#52349=CARTESIAN_POINT('Ctrl Pts',(-20.6981274285326,22.0496064428178,23.8458836531076));
#52350=CARTESIAN_POINT('Ctrl Pts',(-20.6884341524419,22.0681756415642,23.8472040005109));
#52351=CARTESIAN_POINT('Ctrl Pts',(-20.6770655663065,22.0904816784908,23.8487687038613));
#52352=CARTESIAN_POINT('Ctrl Pts',(-20.6752157478452,22.094128301454,23.849023826549));
#52353=CARTESIAN_POINT('Ctrl Pts',(-20.6723698355491,22.0997651299382,23.8494171302534));
#52354=CARTESIAN_POINT('Ctrl Pts',(-20.6713688630932,22.1017528464478,23.8495556185961));
#52355=CARTESIAN_POINT('Ctrl Pts',(-20.6696162227746,22.1052422071154,23.8497983724419));
#52356=CARTESIAN_POINT('Ctrl Pts',(-20.668863672581,22.1067433959352,23.8499026937576));
#52357=CARTESIAN_POINT('Ctrl Pts',(-20.6672718684488,22.1099249350251,23.8501235411501));
#52358=CARTESIAN_POINT('Ctrl Pts',(-20.6664329125861,22.1116054259506,23.8502400481008));
#52359=CARTESIAN_POINT('Ctrl Pts',(-20.6640523730453,22.116384273115,23.8505709527065));
#52360=CARTESIAN_POINT('Ctrl Pts',(-20.6625143042087,22.1194843923606,23.8507851283171));
#52361=CARTESIAN_POINT('Ctrl Pts',(-20.6560277947913,22.1326116165875,23.8516900018728));
#52362=CARTESIAN_POINT('Ctrl Pts',(-20.651126486011,22.1426621183294,23.8523777713307));
#52363=CARTESIAN_POINT('Ctrl Pts',(-20.562146759046,22.3275581733677,23.8649422237144));
#52364=CARTESIAN_POINT('Ctrl Pts',(-20.4939597164943,22.5096486669378,23.8758840789047));
#52365=CARTESIAN_POINT('Ctrl Pts',(-20.4050022469722,22.8335681701034,23.8946876630477));
#52366=CARTESIAN_POINT('Ctrl Pts',(-20.3765109827375,22.9726721133462,23.9025639437096));
#52367=CARTESIAN_POINT('Ctrl Pts',(-20.3412183565413,23.2305073460493,23.917354402804));
#52368=CARTESIAN_POINT('Ctrl Pts',(-20.3316393381261,23.3486036678032,23.9241997599347));
#52369=CARTESIAN_POINT('Ctrl Pts',(-20.3277034743309,23.5008236176375,23.9332625908732));
#52370=CARTESIAN_POINT('Ctrl Pts',(-20.3273619299407,23.5347063536578,23.93529475094));
#52371=CARTESIAN_POINT('Ctrl Pts',(-20.3276335067348,23.5824414824083,23.9381812226157));
#52372=CARTESIAN_POINT('Ctrl Pts',(-20.3278016631737,23.596294895558,23.9390217017117));
#52373=CARTESIAN_POINT('Ctrl Pts',(-20.328250771991,23.6204561324949,23.9404925900669));
#52374=CARTESIAN_POINT('Ctrl Pts',(-20.3284918804015,23.6307645618137,23.9411217471603));
#52375=CARTESIAN_POINT('Ctrl Pts',(-20.3289114426044,23.645646983032,23.9420324372125));
#52376=CARTESIAN_POINT('Ctrl Pts',(-20.3290501788638,23.6502221039739,23.942312722607));
#52377=CARTESIAN_POINT('Ctrl Pts',(-20.3293096299157,23.6582158951931,23.9428030159618));
#52378=CARTESIAN_POINT('Ctrl Pts',(-20.3294260421854,23.6616347057942,23.943012888473));
#52379=CARTESIAN_POINT('Ctrl Pts',(-20.3296599799454,23.6681977658456,23.9434161312249));
#52380=CARTESIAN_POINT('Ctrl Pts',(-20.3297766673575,23.6713420429934,23.9436094749067));
#52381=CARTESIAN_POINT('Ctrl Pts',(-20.3300618009526,23.6787332097376,23.9440643299999));
#52382=CARTESIAN_POINT('Ctrl Pts',(-20.3302340438858,23.6829799398966,23.9443259604852));
#52383=CARTESIAN_POINT('Ctrl Pts',(-20.3308553244439,23.6975843613215,23.9452266912823));
#52384=CARTESIAN_POINT('Ctrl Pts',(-20.3313459376159,23.7079401362737,23.9458670968083));
#52385=CARTESIAN_POINT('Ctrl Pts',(-20.3374300734454,23.8244653107288,23.9530926681313));
#52386=CARTESIAN_POINT('Ctrl Pts',(-20.3482233794895,23.9302864949458,23.9598411103387));
#52387=CARTESIAN_POINT('Ctrl Pts',(-20.4100764883942,24.3365077697871,23.986511281385));
#52388=CARTESIAN_POINT('Ctrl Pts',(-20.4983943960213,24.629609982848,24.0075733636155));
#52389=CARTESIAN_POINT('Ctrl Pts',(-20.6563287677979,24.9702367166931,24.0324797284));
#52390=CARTESIAN_POINT('Ctrl Pts',(-20.6882877534216,25.0335963876198,24.037122198929));
#52391=CARTESIAN_POINT('Ctrl Pts',(-20.7365061926084,25.1218201403493,24.043549625663));
#52392=CARTESIAN_POINT('Ctrl Pts',(-20.751055515842,25.14759076436,24.0454224511347));
#52393=CARTESIAN_POINT('Ctrl Pts',(-20.7682199751146,25.1770384999244,24.0475538796328));
#52394=CARTESIAN_POINT('Ctrl Pts',(-20.770489708622,25.1809138638992,24.0478342047037));
#52395=CARTESIAN_POINT('Ctrl Pts',(-20.7739396541395,25.1867761976131,24.0482579787291));
#52396=CARTESIAN_POINT('Ctrl Pts',(-20.7751139026096,25.1887666429034,24.0484018144353));
#52397=CARTESIAN_POINT('Ctrl Pts',(-20.7771491719011,25.1922081234281,24.0486504195823));
#52398=CARTESIAN_POINT('Ctrl Pts',(-20.7780091897232,25.1936597430291,24.0487552545951));
#52399=CARTESIAN_POINT('Ctrl Pts',(-20.7798048258241,25.1966851673447,24.0489736922917));
#52400=CARTESIAN_POINT('Ctrl Pts',(-20.7807406426868,25.1982588458151,24.0490872812649));
#52401=CARTESIAN_POINT('Ctrl Pts',(-20.7833288643433,25.2026027930929,24.0494007446474));
#52402=CARTESIAN_POINT('Ctrl Pts',(-20.784984093795,25.2053713896216,24.0496004335171));
#52403=CARTESIAN_POINT('Ctrl Pts',(-20.7914713718626,25.2161853487183,24.0503800497664));
#52404=CARTESIAN_POINT('Ctrl Pts',(-20.7963344595317,25.2242121774625,24.0509579614318));
#52405=CARTESIAN_POINT('Ctrl Pts',(-20.8823241903912,25.364754608552,24.0610651932127));
#52406=CARTESIAN_POINT('Ctrl Pts',(-20.9729073110434,25.4912742656986,24.0699882979585));
#52407=CARTESIAN_POINT('Ctrl Pts',(-21.1933294000038,25.7563521572139,24.0894320316263));
#52408=CARTESIAN_POINT('Ctrl Pts',(-21.3269694692907,25.8909736204585,24.0998531585584));
#52409=CARTESIAN_POINT('Ctrl Pts',(-21.5267954118918,26.0596239943845,24.1147436687288));
#52410=CARTESIAN_POINT('Ctrl Pts',(-21.5834808218823,26.1042948161991,24.1188974046921));
#52411=CARTESIAN_POINT('Ctrl Pts',(-21.7063662386689,26.1946160858944,24.1278169050986));
#52412=CARTESIAN_POINT('Ctrl Pts',(-21.7728699245907,26.2397663697276,24.1325955088226));
#52413=CARTESIAN_POINT('Ctrl Pts',(-21.8497801360932,26.2878826687771,24.1380990118875));
#52414=CARTESIAN_POINT('Ctrl Pts',(-21.8585993466416,26.2933410525492,24.1387297456947));
#52415=CARTESIAN_POINT('Ctrl Pts',(-21.8743988748986,26.3030145216435,24.1398591568115));
#52416=CARTESIAN_POINT('Ctrl Pts',(-21.881369160575,26.3072458838771,24.1403572325108));
#52417=CARTESIAN_POINT('Ctrl Pts',(-21.8919113215309,26.3135909507984,24.1411102905615));
#52418=CARTESIAN_POINT('Ctrl Pts',(-21.8954713811887,26.3157243054611,24.1413645528743));
#52419=CARTESIAN_POINT('Ctrl Pts',(-21.9016476354321,26.3194092102352,24.1418055949037));
#52420=CARTESIAN_POINT('Ctrl Pts',(-21.9042619298394,26.3209639480615,24.1419922578709));
#52421=CARTESIAN_POINT('Ctrl Pts',(-21.9096447327773,26.3241548288673,24.1423765514942));
#52422=CARTESIAN_POINT('Ctrl Pts',(-21.9124134965096,26.3257905333864,24.1425741978904));
#52423=CARTESIAN_POINT('Ctrl Pts',(-21.9198579987277,26.3301735088906,24.1431055584493));
#52424=CARTESIAN_POINT('Ctrl Pts',(-21.9245382158995,26.3329131174339,24.1434395508876));
#52425=CARTESIAN_POINT('Ctrl Pts',(-21.9416374542388,26.3428644518291,24.1446595814824));
#52426=CARTESIAN_POINT('Ctrl Pts',(-21.9540975859397,26.3500048747246,24.1455481993334));
#52427=CARTESIAN_POINT('Ctrl Pts',(-22.0023892250627,26.3772518079234,24.1489909243063));
#52428=CARTESIAN_POINT('Ctrl Pts',(-22.0385399192203,26.3967464445293,24.1515654718717));
#52429=CARTESIAN_POINT('Ctrl Pts',(-22.0750361722079,26.4155368553179,24.1541632309577));
#52430=CARTESIAN_POINT('Origin',(-23.5502525316942,23.5502525316942,-77.3107734492734));
#52431=CARTESIAN_POINT('',(-22.0750360153461,26.4155367745563,25.653793035611));
#52432=CARTESIAN_POINT('',(-22.0750361607755,26.4155368494319,25.4084140214669));
#52433=CARTESIAN_POINT('',(-22.0750360153461,26.4155367745563,-77.3107734492734));
#52434=CARTESIAN_POINT('',(-26.7730020784469,23.5485433198117,24.8107734492728));
#52435=CARTESIAN_POINT('Ctrl Pts',(-26.7730020784469,23.5485433198117,24.8107734492728));
#52436=CARTESIAN_POINT('Ctrl Pts',(-26.7729503115416,23.450935894898,24.8168290675995));
#52437=CARTESIAN_POINT('Ctrl Pts',(-26.7684646036353,23.3534486965496,24.8228846859262));
#52438=CARTESIAN_POINT('Ctrl Pts',(-26.7595750669373,23.2563708764643,24.8289403042529));
#52439=CARTESIAN_POINT('Ctrl Pts',(-26.7505145500469,23.1574258742166,24.8351123955547));
#52440=CARTESIAN_POINT('Ctrl Pts',(-26.736858003116,23.0587260119028,24.8412844868565));
#52441=CARTESIAN_POINT('Ctrl Pts',(-26.7186249230167,22.9607324282157,24.8474565781583));
#52442=CARTESIAN_POINT('Ctrl Pts',(-26.7004165469383,22.8628716161464,24.8536203068866));
#52443=CARTESIAN_POINT('Ctrl Pts',(-26.6776440411043,22.765715603996,24.8597840356149));
#52444=CARTESIAN_POINT('Ctrl Pts',(-26.6503787403315,22.6697214118465,24.8659477643432));
#52445=CARTESIAN_POINT('Ctrl Pts',(-26.6231423245858,22.5738289165339,24.8721049631794));
#52446=CARTESIAN_POINT('Ctrl Pts',(-26.5914226946394,22.4790962097682,24.8782621620156));
#52447=CARTESIAN_POINT('Ctrl Pts',(-26.5553422294784,22.3859701472311,24.8844193608518));
#52448=CARTESIAN_POINT('Ctrl Pts',(-26.519288136949,22.2929121541969,24.8905720591492));
#52449=CARTESIAN_POINT('Ctrl Pts',(-26.4788797029659,22.2014588744071,24.8967247574465));
#52450=CARTESIAN_POINT('Ctrl Pts',(-26.4342888589272,22.112041133568,24.9028774557439));
#52451=CARTESIAN_POINT('Ctrl Pts',(-26.3897149237996,22.0226573000625,24.9090278209293));
#52452=CARTESIAN_POINT('Ctrl Pts',(-26.3409619235781,21.9353078601051,24.9151781861148));
#52453=CARTESIAN_POINT('Ctrl Pts',(-26.2882491878679,21.8504019872987,24.9213285513003));
#52454=CARTESIAN_POINT('Ctrl Pts',(-26.2355423386933,21.7655055960994,24.9274782296622));
#52455=CARTESIAN_POINT('Ctrl Pts',(-26.1788768622937,21.6830525985938,24.9336279080242));
#52456=CARTESIAN_POINT('Ctrl Pts',(-26.1185166255224,21.6034250850896,24.9397775863862));
#52457=CARTESIAN_POINT('Ctrl Pts',(-26.0581469812845,21.5237851612106,24.9459282232086));
#52458=CARTESIAN_POINT('Ctrl Pts',(-25.9940816953355,21.4469719422293,24.9520788600309));
#52459=CARTESIAN_POINT('Ctrl Pts',(-25.926625675243,21.3733353892379,24.9582294968532));
#52460=CARTESIAN_POINT('Ctrl Pts',(-25.8590974913771,21.299620060601,24.9643867135651));
#52461=CARTESIAN_POINT('Ctrl Pts',(-25.7881716238659,21.229088505097,24.9705439302769));
#52462=CARTESIAN_POINT('Ctrl Pts',(-25.7141906149643,21.1620545637122,24.9767011469888));
#52463=CARTESIAN_POINT('Ctrl Pts',(-25.6401683323597,21.0949832243651,24.9828617987868));
#52464=CARTESIAN_POINT('Ctrl Pts',(-25.5630878491221,21.0314136615306,24.9890224505847));
#52465=CARTESIAN_POINT('Ctrl Pts',(-25.4833239940354,20.9716187298561,24.9951831023827));
#52466=CARTESIAN_POINT('Ctrl Pts',(-25.4034266656512,20.9117237399949,25.0013540631421));
#52467=CARTESIAN_POINT('Ctrl Pts',(-25.3208373557785,20.8556162421793,25.0075250239016));
#52468=CARTESIAN_POINT('Ctrl Pts',(-25.2359591145877,20.8035252283585,25.013695984661));
#52469=CARTESIAN_POINT('Ctrl Pts',(-25.1711699579192,20.7637631785316,25.0184063949833));
#52470=CARTESIAN_POINT('Ctrl Pts',(-25.1050477273011,20.7263404488991,25.0231168053055));
#52471=CARTESIAN_POINT('Ctrl Pts',(-25.037779847147,20.691340142641,25.0278272156278));
#52472=CARTESIAN_POINT('Ctrl Pts',(-24.9496381631259,20.645478939229,25.0339993069332));
#52473=CARTESIAN_POINT('Ctrl Pts',(-24.8592183703656,20.6036169615311,25.0401713982386));
#52474=CARTESIAN_POINT('Ctrl Pts',(-24.7669189714713,20.5659870715147,25.046343489544));
#52475=CARTESIAN_POINT('Ctrl Pts',(-24.6747446291396,20.5284081662799,25.0525072182757));
#52476=CARTESIAN_POINT('Ctrl Pts',(-24.5806961411827,20.4950501142229,25.0586709470075));
#52477=CARTESIAN_POINT('Ctrl Pts',(-24.4851965657563,20.4660999388947,25.0648346757392));
#52478=CARTESIAN_POINT('Ctrl Pts',(-24.3897981631688,20.4371804335608,25.0709918745787));
#52479=CARTESIAN_POINT('Ctrl Pts',(-24.2929521428106,20.4126596464327,25.0771490734183));
#52480=CARTESIAN_POINT('Ctrl Pts',(-24.1951006028942,20.3926761624563,25.0833062722578));
#52481=CARTESIAN_POINT('Ctrl Pts',(-24.0973205865218,20.3727072851953,25.0894589705582));
#52482=CARTESIAN_POINT('Ctrl Pts',(-23.9985369361751,20.3572692039967,25.0956116688586));
#52483=CARTESIAN_POINT('Ctrl Pts',(-23.8992050489584,20.3464501496496,25.101764367159));
#52484=CARTESIAN_POINT('Ctrl Pts',(-23.7999108285361,20.3356351979034,25.1079147323474));
#52485=CARTESIAN_POINT('Ctrl Pts',(-23.7000692156912,20.3294358396973,25.1140650975358));
#52486=CARTESIAN_POINT('Ctrl Pts',(-23.6001430119909,20.3278887250337,25.1202154627242));
#52487=CARTESIAN_POINT('Ctrl Pts',(-23.5002279672502,20.3263417831394,25.126365141089));
#52488=CARTESIAN_POINT('Ctrl Pts',(-23.400228784785,20.3294460586256,25.1325148194537));
#52489=CARTESIAN_POINT('Ctrl Pts',(-23.3006095548028,20.3371860918911,25.1386644978185));
#52490=CARTESIAN_POINT('Ctrl Pts',(-23.2009747986322,20.3449273314821,25.1448151346435));
#52491=CARTESIAN_POINT('Ctrl Pts',(-23.1017205457037,20.3573057302842,25.1509657714684));
#52492=CARTESIAN_POINT('Ctrl Pts',(-23.0033060396225,20.3742539332514,25.1571164082933));
#52493=CARTESIAN_POINT('Ctrl Pts',(-22.9047862506941,20.3912202672355,25.1632736250076));
#52494=CARTESIAN_POINT('Ctrl Pts',(-22.8071084314714,20.412766093829,25.1694308417219));
#52495=CARTESIAN_POINT('Ctrl Pts',(-22.7107217802524,20.4387728708441,25.1755880584361));
#52496=CARTESIAN_POINT('Ctrl Pts',(-22.614281355316,20.4647941569335,25.1817487102363));
#52497=CARTESIAN_POINT('Ctrl Pts',(-22.5191339466243,20.4952812171865,25.1879093620365));
#52498=CARTESIAN_POINT('Ctrl Pts',(-22.4257117222186,20.5300661913629,25.1940700138367));
#52499=CARTESIAN_POINT('Ctrl Pts',(-22.3321331692098,20.5649093731708,25.2002409745982));
#52500=CARTESIAN_POINT('Ctrl Pts',(-22.2402859666905,20.6040646641897,25.2064119353597));
#52501=CARTESIAN_POINT('Ctrl Pts',(-22.150580635134,20.6473167514056,25.2125828961211));
#52502=CARTESIAN_POINT('Ctrl Pts',(-22.0821068701068,20.6803318822298,25.2172933064149));
#52503=CARTESIAN_POINT('Ctrl Pts',(-22.0148806314104,20.7157330522426,25.2220037167087));
#52504=CARTESIAN_POINT('Ctrl Pts',(-21.9490731459827,20.7534074989345,25.2267141270025));
#52505=CARTESIAN_POINT('Ctrl Pts',(-21.862845028446,20.8027726524025,25.232886218366));
#52506=CARTESIAN_POINT('Ctrl Pts',(-21.7787501123152,20.8562161680798,25.2390583097295));
#52507=CARTESIAN_POINT('Ctrl Pts',(-21.6971997158266,20.9135286507948,25.245230401093));
#52508=CARTESIAN_POINT('Ctrl Pts',(-21.6157598120601,20.9707634807638,25.251394129883));
#52509=CARTESIAN_POINT('Ctrl Pts',(-21.5368579277957,21.0318566110277,25.2575578586731));
#52510=CARTESIAN_POINT('Ctrl Pts',(-21.4608800899563,21.0965532098118,25.2637215874632));
#52511=CARTESIAN_POINT('Ctrl Pts',(-21.3849827435036,21.1611812686229,25.2698787863612));
#52512=CARTESIAN_POINT('Ctrl Pts',(-21.3120036137762,21.2294049262685,25.2760359852593));
#52513=CARTESIAN_POINT('Ctrl Pts',(-21.2422982674428,21.3009271491353,25.2821931841574));
#52514=CARTESIAN_POINT('Ctrl Pts',(-21.1726438714911,21.3723970935938,25.2883458825164));
#52515=CARTESIAN_POINT('Ctrl Pts',(-21.1062588036481,21.4471604995426,25.2944985808754));
#52516=CARTESIAN_POINT('Ctrl Pts',(-21.0434634554003,21.5248819262312,25.3006512792344));
#52517=CARTESIAN_POINT('Ctrl Pts',(-20.9806919192384,21.6025738808436,25.3068016444814));
#52518=CARTESIAN_POINT('Ctrl Pts',(-20.9215076706287,21.6832212898979,25.3129520097284));
#52519=CARTESIAN_POINT('Ctrl Pts',(-20.8661917077021,21.7664546015432,25.3191023749753));
#52520=CARTESIAN_POINT('Ctrl Pts',(-20.8108819220205,21.8496786183571,25.3252520533987));
#52521=CARTESIAN_POINT('Ctrl Pts',(-20.759439803631,21.9354876018513,25.331401731822));
#52522=CARTESIAN_POINT('Ctrl Pts',(-20.7121032065455,22.023482748571,25.3375514102453));
#52523=CARTESIAN_POINT('Ctrl Pts',(-20.6647592317998,22.1114916098019,25.3437020471287));
#52524=CARTESIAN_POINT('Ctrl Pts',(-20.6215222551146,22.2016869284285,25.349852684012));
#52525=CARTESIAN_POINT('Ctrl Pts',(-20.5825838501992,22.2936459268358,25.3560033208954));
#52526=CARTESIAN_POINT('Ctrl Pts',(-20.5436037893743,22.3857033020442,25.3621605376676));
#52527=CARTESIAN_POINT('Ctrl Pts',(-20.5089316529185,22.4795277239199,25.3683177544397));
#52528=CARTESIAN_POINT('Ctrl Pts',(-20.4787105200252,22.5746771973133,25.3744749712119));
#52529=CARTESIAN_POINT('Ctrl Pts',(-20.4484725268871,22.6698797542037,25.3806356230698));
#52530=CARTESIAN_POINT('Ctrl Pts',(-20.422690594659,22.7664084150925,25.3867962749276));
#52531=CARTESIAN_POINT('Ctrl Pts',(-20.4014571048539,22.8638088541726,25.3929569267855));
#52532=CARTESIAN_POINT('Ctrl Pts',(-20.3801880838731,22.9613722788071,25.3991278876037));
#52533=CARTESIAN_POINT('Ctrl Pts',(-20.3634827811419,23.0598099670568,25.4052988484219));
#52534=CARTESIAN_POINT('Ctrl Pts',(-20.3513819539305,23.1586601553409,25.41146980924));
#52535=CARTESIAN_POINT('Ctrl Pts',(-20.3421451663856,23.2341143513231,25.4161802189525));
#52536=CARTESIAN_POINT('Ctrl Pts',(-20.3355901338506,23.3098087377366,25.420890628665));
#52537=CARTESIAN_POINT('Ctrl Pts',(-20.3317145427561,23.385538305647,25.4256010383775));
#52538=CARTESIAN_POINT('Ctrl Pts',(-20.3266363216934,23.4847674238516,25.4317731296101));
#52539=CARTESIAN_POINT('Ctrl Pts',(-20.326142380789,23.584406371618,25.4379452208428));
#52540=CARTESIAN_POINT('Ctrl Pts',(-20.3302788873238,23.6839959130626,25.4441173120754));
#52541=CARTESIAN_POINT('Ctrl Pts',(-20.3344097893012,23.7834505205247,25.4502810407347));
#52542=CARTESIAN_POINT('Ctrl Pts',(-20.3431586510069,23.8828554245149,25.4564447693939));
#52543=CARTESIAN_POINT('Ctrl Pts',(-20.3565197421183,23.9817481067446,25.4626084980532));
#52544=CARTESIAN_POINT('Ctrl Pts',(-20.369866678408,24.0805360214613,25.4687656968205));
#52545=CARTESIAN_POINT('Ctrl Pts',(-20.3878160720054,24.1788123651428,25.4749228955879));
#52546=CARTESIAN_POINT('Ctrl Pts',(-20.410310222414,24.2761174343394,25.4810800943553));
#52547=CARTESIAN_POINT('Ctrl Pts',(-20.4327879309649,24.3733513794407,25.4872327925843));
#52548=CARTESIAN_POINT('Ctrl Pts',(-20.4598036942034,24.4696150395802,25.4933854908134));
#52549=CARTESIAN_POINT('Ctrl Pts',(-20.4912484853867,24.5644575440928,25.4995381890424));
#52550=CARTESIAN_POINT('Ctrl Pts',(-20.5226813526625,24.6592640841989,25.50568855416));
#52551=CARTESIAN_POINT('Ctrl Pts',(-20.5585397741922,24.7526501276034,25.5118389192775));
#52552=CARTESIAN_POINT('Ctrl Pts',(-20.5986647312134,24.8441795074362,25.517989284395));
#52553=CARTESIAN_POINT('Ctrl Pts',(-20.6387852074039,24.9356986660081,25.5241389626895));
#52554=CARTESIAN_POINT('Ctrl Pts',(-20.6831710974228,25.0253611753709,25.530288640984));
#52555=CARTESIAN_POINT('Ctrl Pts',(-20.731615451417,25.1127513547935,25.5364383192785));
#52556=CARTESIAN_POINT('Ctrl Pts',(-20.7800673557275,25.2001551544512,25.5425889560338));
#52557=CARTESIAN_POINT('Ctrl Pts',(-20.8325787697541,25.2852855407593,25.5487395927892));
#52558=CARTESIAN_POINT('Ctrl Pts',(-20.8888975573152,25.367752810332,25.5548902295445));
#52559=CARTESIAN_POINT('Ctrl Pts',(-20.9452765941619,25.4503083025793,25.5610474461906));
#52560=CARTESIAN_POINT('Ctrl Pts',(-21.00547089264,25.5301946295357,25.5672046628367));
#52561=CARTESIAN_POINT('Ctrl Pts',(-21.0691859351917,25.6070524991727,25.5733618794828));
#52562=CARTESIAN_POINT('Ctrl Pts',(-21.1329365241119,25.6839532475091,25.5795225312156));
#52563=CARTESIAN_POINT('Ctrl Pts',(-21.2002114762874,25.7578218526046,25.5856831829483));
#52564=CARTESIAN_POINT('Ctrl Pts',(-21.2706784959261,25.8283350099974,25.591843834681));
#52565=CARTESIAN_POINT('Ctrl Pts',(-21.3412634319697,25.898966161,25.5980147953769));
#52566=CARTESIAN_POINT('Ctrl Pts',(-21.4150507837403,25.9662303559649,25.6041857560727));
#52567=CARTESIAN_POINT('Ctrl Pts',(-21.4916740928308,26.0298437023404,25.6103567167685));
#52568=CARTESIAN_POINT('Ctrl Pts',(-21.5501621136388,26.0784009725842,25.6150671277631));
#52569=CARTESIAN_POINT('Ctrl Pts',(-21.6103018138662,26.1248318693068,25.6197775387578));
#52570=CARTESIAN_POINT('Ctrl Pts',(-21.6719194653256,26.1690275228468,25.6244879497524));
#52571=CARTESIAN_POINT('Ctrl Pts',(-21.7526486331184,26.2269310333805,25.6306593560061));
#52572=CARTESIAN_POINT('Ctrl Pts',(-21.836199967998,26.2812000499403,25.6368307622599));
#52573=CARTESIAN_POINT('Ctrl Pts',(-21.9222121847103,26.3315475881549,25.6430021685136));
#52574=CARTESIAN_POINT('Ctrl Pts',(-21.9723437301601,26.360892255654,25.6465991242127));
#52575=CARTESIAN_POINT('Ctrl Pts',(-22.0233105772739,26.3889054828269,25.6501960799119));
#52576=CARTESIAN_POINT('Ctrl Pts',(-22.0750360153461,26.4155367745563,25.653793035611));
#52577=CARTESIAN_POINT('Ctrl Pts',(-26.7730020009422,23.5484029475698,24.8083546326523));
#52578=CARTESIAN_POINT('Ctrl Pts',(-26.7731829229496,23.8636447879474,24.7900599457156));
#52579=CARTESIAN_POINT('Ctrl Pts',(-26.7271130127483,24.1772373733017,24.7732082235204));
#52580=CARTESIAN_POINT('Ctrl Pts',(-26.6081560899502,24.5724184315231,24.7492635678694));
#52581=CARTESIAN_POINT('Ctrl Pts',(-26.5758835712151,24.6643222259386,24.7435064575939));
#52582=CARTESIAN_POINT('Ctrl Pts',(-26.5329639705256,24.7708492053277,24.7365476269339));
#52583=CARTESIAN_POINT('Ctrl Pts',(-26.5262925927927,24.7870262793587,24.7354829744732));
#52584=CARTESIAN_POINT('Ctrl Pts',(-26.5172878862852,24.8083665366096,24.7340677738117));
#52585=CARTESIAN_POINT('Ctrl Pts',(-26.5150721265288,24.813579256732,24.7337212336612));
#52586=CARTESIAN_POINT('Ctrl Pts',(-26.5114154033842,24.8221193318752,24.7331520805999));
#52587=CARTESIAN_POINT('Ctrl Pts',(-26.5099825396466,24.8254501594891,24.7329297446674));
#52588=CARTESIAN_POINT('Ctrl Pts',(-26.5071979000963,24.8318933413037,24.732498969244));
#52589=CARTESIAN_POINT('Ctrl Pts',(-26.5058468234619,24.8350059939978,24.7322905539096));
#52590=CARTESIAN_POINT('Ctrl Pts',(-26.5027201488775,24.8421782901962,24.7318095947986));
#52591=CARTESIAN_POINT('Ctrl Pts',(-26.5009410923502,24.8462364103354,24.7315369327176));
#52592=CARTESIAN_POINT('Ctrl Pts',(-26.4953783888303,24.8588543945781,24.7306874711052));
#52593=CARTESIAN_POINT('Ctrl Pts',(-26.491565845879,24.8674013975213,24.7301096798018));
#52594=CARTESIAN_POINT('Ctrl Pts',(-26.4589039024724,24.9397743217212,24.7251966063665));
#52595=CARTESIAN_POINT('Ctrl Pts',(-26.4280199961365,25.0026563250545,24.7207912836801));
#52596=CARTESIAN_POINT('Ctrl Pts',(-26.3911499023996,25.0719262395936,24.71577731142));
#52597=CARTESIAN_POINT('Ctrl Pts',(-26.3871565679271,25.0793582282664,24.7152372472884));
#52598=CARTESIAN_POINT('Ctrl Pts',(-26.3567766719616,25.1353695679733,24.7111510342131));
#52599=CARTESIAN_POINT('Ctrl Pts',(-26.3291744805024,25.1832761114008,24.7075646483272));
#52600=CARTESIAN_POINT('Ctrl Pts',(-26.1644291442531,25.4529273856814,24.6868551744497));
#52601=CARTESIAN_POINT('Ctrl Pts',(-26.002011043197,25.6580817296413,24.6689254480265));
#52602=CARTESIAN_POINT('Ctrl Pts',(-25.7715222255063,25.8860856273245,24.6472869898608));
#52603=CARTESIAN_POINT('Ctrl Pts',(-25.7250329927821,25.9294301611663,24.643087990581));
#52604=CARTESIAN_POINT('Ctrl Pts',(-25.6496876396391,25.9956236121448,24.6365755393889));
#52605=CARTESIAN_POINT('Ctrl Pts',(-25.6216712691363,26.0194005971973,24.6342144210437));
#52606=CARTESIAN_POINT('Ctrl Pts',(-25.583593513431,26.0506121083367,24.6310921866857));
#52607=CARTESIAN_POINT('Ctrl Pts',(-25.5738878101214,26.0584737803422,24.6303037378344));
#52608=CARTESIAN_POINT('Ctrl Pts',(-25.5576061972556,26.0715059480572,24.6289937119343));
#52609=CARTESIAN_POINT('Ctrl Pts',(-25.5510555165781,26.0767075476308,24.6284700153822));
#52610=CARTESIAN_POINT('Ctrl Pts',(-25.5421490689468,26.0837233893494,24.6277626322869));
#52611=CARTESIAN_POINT('Ctrl Pts',(-25.5398110097781,26.0855599024408,24.6275773666569));
#52612=CARTESIAN_POINT('Ctrl Pts',(-25.5360948401269,26.0884705959114,24.6272835900863));
#52613=CARTESIAN_POINT('Ctrl Pts',(-25.5347183990394,26.0895468897506,24.6271749272451));
#52614=CARTESIAN_POINT('Ctrl Pts',(-25.5318555171133,26.0917817411305,24.6269492300012));
#52615=CARTESIAN_POINT('Ctrl Pts',(-25.5303689392054,26.0929401111973,24.6268322095589));
#52616=CARTESIAN_POINT('Ctrl Pts',(-25.5269558502869,26.0955948472363,24.6265639374704));
#52617=CARTESIAN_POINT('Ctrl Pts',(-25.5250286514086,26.0970903337783,24.6264127491369));
#52618=CARTESIAN_POINT('Ctrl Pts',(-25.5189367888999,26.1018064846637,24.6259357566268));
#52619=CARTESIAN_POINT('Ctrl Pts',(-25.5147659030678,26.1050191539337,24.6256105215025));
#52620=CARTESIAN_POINT('Ctrl Pts',(-25.4801134198738,26.1315755584305,24.6229193670571));
#52621=CARTESIAN_POINT('Ctrl Pts',(-25.4492231531455,26.154384347586,24.6205905337262));
#52622=CARTESIAN_POINT('Ctrl Pts',(-25.4083916698818,26.1834204948443,24.6175919183136));
#52623=CARTESIAN_POINT('Ctrl Pts',(-25.3988153110416,26.190152195999,24.6168942450292));
#52624=CARTESIAN_POINT('Ctrl Pts',(-25.3831371613361,26.2010460061342,24.6157607632035));
#52625=CARTESIAN_POINT('Ctrl Pts',(-25.3770574492587,26.205239519366,24.6153233414309));
#52626=CARTESIAN_POINT('Ctrl Pts',(-25.2872292634605,26.26674434496,24.6088907718959));
#52627=CARTESIAN_POINT('Ctrl Pts',(-25.2008271021701,26.3200941762613,24.603090576683));
#52628=CARTESIAN_POINT('Ctrl Pts',(-25.0500311775264,26.4036378361574,24.5933620074062));
#52629=CARTESIAN_POINT('Ctrl Pts',(-24.9868994038662,26.43593958656,24.5893994834452));
#52630=CARTESIAN_POINT('Ctrl Pts',(-24.783229503671,26.5318066703035,24.5768211899159));
#52631=CARTESIAN_POINT('Ctrl Pts',(-24.639177555762,26.5873787958498,24.5682156958418));
#52632=CARTESIAN_POINT('Ctrl Pts',(-24.3825066355611,26.6657795148598,24.5527578007421));
#52633=CARTESIAN_POINT('Ctrl Pts',(-24.2716200106518,26.6933051675425,24.5460439215414));
#52634=CARTESIAN_POINT('Ctrl Pts',(-24.1405303566504,26.7185428319792,24.5379638604057));
#52635=CARTESIAN_POINT('Ctrl Pts',(-24.1215135510899,26.7220268237688,24.5367883612839));
#52636=CARTESIAN_POINT('Ctrl Pts',(-24.0966742280309,26.7263469040183,24.5352482350452));
#52637=CARTESIAN_POINT('Ctrl Pts',(-24.0908788742407,26.7273385061615,24.5348885689008));
#52638=CARTESIAN_POINT('Ctrl Pts',(-24.0814579094915,26.7289239375919,24.5343033402141));
#52639=CARTESIAN_POINT('Ctrl Pts',(-24.0778339214935,26.7295274391271,24.5340780858782));
#52640=CARTESIAN_POINT('Ctrl Pts',(-24.0708772729198,26.7306737054647,24.533645427159));
#52641=CARTESIAN_POINT('Ctrl Pts',(-24.0675447739702,26.7312174324258,24.5334380536958));
#52642=CARTESIAN_POINT('Ctrl Pts',(-24.0599433036526,26.7324454189734,24.5329647708083));
#52643=CARTESIAN_POINT('Ctrl Pts',(-24.0556738041121,26.7331263262337,24.5326987551748));
#52644=CARTESIAN_POINT('Ctrl Pts',(-24.042365958612,26.7352212330773,24.5318690028271));
#52645=CARTESIAN_POINT('Ctrl Pts',(-24.0333230126722,26.7366053309589,24.5313043174583));
#52646=CARTESIAN_POINT('Ctrl Pts',(-23.9630465829505,26.7470556805904,24.5269091364839));
#52647=CARTESIAN_POINT('Ctrl Pts',(-23.9015729284183,26.7543939799702,24.5230241643808));
#52648=CARTESIAN_POINT('Ctrl Pts',(-23.8348940360998,26.7604117703565,24.5187625207856));
#52649=CARTESIAN_POINT('Ctrl Pts',(-23.8298576630376,26.7608543590255,24.5184403404906));
#52650=CARTESIAN_POINT('Ctrl Pts',(-23.802907893282,26.7631587697666,24.5167147847664));
#52651=CARTESIAN_POINT('Ctrl Pts',(-23.7809773232093,26.7648080623732,24.5153050783406));
#52652=CARTESIAN_POINT('Ctrl Pts',(-23.5035062614069,26.7828213143613,24.497399136189));
#52653=CARTESIAN_POINT('Ctrl Pts',(-23.246944905116,26.7688937132499,24.4799839898157));
#52654=CARTESIAN_POINT('Ctrl Pts',(-22.8890453021343,26.7062700769006,24.4554642681914));
#52655=CARTESIAN_POINT('Ctrl Pts',(-22.7842835862117,26.6824940069301,24.448274714745));
#52656=CARTESIAN_POINT('Ctrl Pts',(-22.6413059934595,26.6424401479014,24.4386003177503));
#52657=CARTESIAN_POINT('Ctrl Pts',(-22.6019282340121,26.6305917090377,24.4359509820921));
#52658=CARTESIAN_POINT('Ctrl Pts',(-22.5498718007017,26.6138354034694,24.4324784842278));
#52659=CARTESIAN_POINT('Ctrl Pts',(-22.5369837087975,26.6095968939198,24.4316212278387));
#52660=CARTESIAN_POINT('Ctrl Pts',(-22.5184326885527,26.6033659262793,24.4303912470133));
#52661=CARTESIAN_POINT('Ctrl Pts',(-22.5127481654279,26.6014389042765,24.4300148851612));
#52662=CARTESIAN_POINT('Ctrl Pts',(-22.5026546478469,26.597985788319,24.4293476087184));
#52663=CARTESIAN_POINT('Ctrl Pts',(-22.4982435413587,26.5964659869013,24.4290563322886));
#52664=CARTESIAN_POINT('Ctrl Pts',(-22.4916298657739,26.5941712338393,24.4286201407113));
#52665=CARTESIAN_POINT('Ctrl Pts',(-22.4894248377134,26.5934034674573,24.428474800416));
#52666=CARTESIAN_POINT('Ctrl Pts',(-22.4854981444806,26.5920314497977,24.4282161388622));
#52667=CARTESIAN_POINT('Ctrl Pts',(-22.48377615948,26.5914281332143,24.4281027618608));
#52668=CARTESIAN_POINT('Ctrl Pts',(-22.4803287604498,26.5902170105416,24.4278758921971));
#52669=CARTESIAN_POINT('Ctrl Pts',(-22.4786033575071,26.5896091998778,24.4277624003191));
#52670=CARTESIAN_POINT('Ctrl Pts',(-22.4738440777874,26.587928083693,24.4274494985629));
#52671=CARTESIAN_POINT('Ctrl Pts',(-22.4708112790477,26.5868516987154,24.4272502731076));
#52672=CARTESIAN_POINT('Ctrl Pts',(-22.4589889621292,26.5826358346145,24.4264742974844));
#52673=CARTESIAN_POINT('Ctrl Pts',(-22.450211374184,26.5794626813791,24.4258995393776));
#52674=CARTESIAN_POINT('Ctrl Pts',(-22.3160453566838,26.5303007507336,24.4171335696966));
#52675=CARTESIAN_POINT('Ctrl Pts',(-22.1936747191441,26.4766189517593,24.4093940250471));
#52676=CARTESIAN_POINT('Ctrl Pts',(-22.0750358518511,26.4155366903795,24.4018187331506));
#52677=CARTESIAN_POINT('Ctrl Pts',(-22.0750361722079,26.4155368553179,24.1541632309577));
#52678=CARTESIAN_POINT('Ctrl Pts',(-22.2447100853409,26.5028949336658,24.1662404145976));
#52679=CARTESIAN_POINT('Ctrl Pts',(-22.4218508058323,26.5750313572462,24.1788526081293));
#52680=CARTESIAN_POINT('Ctrl Pts',(-22.72466923503,26.6680019667534,24.2001947943061));
#52681=CARTESIAN_POINT('Ctrl Pts',(-22.8470106117513,26.6978547808728,24.2087525403761));
#52682=CARTESIAN_POINT('Ctrl Pts',(-23.0398027584921,26.7330942509945,24.2219317630653));
#52683=CARTESIAN_POINT('Ctrl Pts',(-23.1092192415935,26.7434532776121,24.2266152637563));
#52684=CARTESIAN_POINT('Ctrl Pts',(-23.2470672325462,26.759442854602,24.2357319232465));
#52685=CARTESIAN_POINT('Ctrl Pts',(-23.3154538668281,26.7651701146984,24.2401660867381));
#52686=CARTESIAN_POINT('Ctrl Pts',(-23.3949764318985,26.7692785041857,24.2451808350332));
#52687=CARTESIAN_POINT('Ctrl Pts',(-23.4059791595261,26.7697903993414,24.2458715332543));
#52688=CARTESIAN_POINT('Ctrl Pts',(-23.4202837255786,26.770382432114,24.246765233302));
#52689=CARTESIAN_POINT('Ctrl Pts',(-23.4235831928683,26.7705139100571,24.2469710773621));
#52690=CARTESIAN_POINT('Ctrl Pts',(-23.428932444153,26.7707188342289,24.2473043163164));
#52691=CARTESIAN_POINT('Ctrl Pts',(-23.4309820956735,26.7707953947145,24.2474318867301));
#52692=CARTESIAN_POINT('Ctrl Pts',(-23.4349170636705,26.7709386156126,24.2476765759008));
#52693=CARTESIAN_POINT('Ctrl Pts',(-23.4368023600201,26.7710055771622,24.2477937111044));
#52694=CARTESIAN_POINT('Ctrl Pts',(-23.441137449412,26.7711557388236,24.2480628290084));
#52695=CARTESIAN_POINT('Ctrl Pts',(-23.4435872853156,26.7712377996191,24.2482147470742));
#52696=CARTESIAN_POINT('Ctrl Pts',(-23.4513613076727,26.7714893227218,24.2486963084999));
#52697=CARTESIAN_POINT('Ctrl Pts',(-23.4566858572178,26.7716483807711,24.2490253671839));
#52698=CARTESIAN_POINT('Ctrl Pts',(-23.5020002689835,26.7728895943084,24.2518194415279));
#52699=CARTESIAN_POINT('Ctrl Pts',(-23.5420089029944,26.7732403257166,24.254244158474));
#52700=CARTESIAN_POINT('Ctrl Pts',(-23.5894453648174,26.7727727700537,24.2570799273101));
#52701=CARTESIAN_POINT('Ctrl Pts',(-23.5968746210305,26.7726738492105,24.2575229132003));
#52702=CARTESIAN_POINT('Ctrl Pts',(-23.6065794133295,26.7725110604257,24.2581001732299));
#52703=CARTESIAN_POINT('Ctrl Pts',(-23.608855256234,26.7724704734712,24.2582354435308));
#52704=CARTESIAN_POINT('Ctrl Pts',(-23.6170346415687,26.7723159353245,24.2587212473545));
#52705=CARTESIAN_POINT('Ctrl Pts',(-23.6229379451371,26.7721881702241,24.2590711960261));
#52706=CARTESIAN_POINT('Ctrl Pts',(-23.6326697540266,26.7719507846003,24.2596470422848));
#52707=CARTESIAN_POINT('Ctrl Pts',(-23.6364984508115,26.771850562641,24.2598733225294));
#52708=CARTESIAN_POINT('Ctrl Pts',(-23.6622200022581,26.7711313756353,24.261391736511));
#52709=CARTESIAN_POINT('Ctrl Pts',(-23.6841067098141,26.7702960629841,24.2626752118637));
#52710=CARTESIAN_POINT('Ctrl Pts',(-23.7409124127531,26.7675478622886,24.2659880224285));
#52711=CARTESIAN_POINT('Ctrl Pts',(-23.7758123407182,26.7652895992896,24.2680052869893));
#52712=CARTESIAN_POINT('Ctrl Pts',(-23.9444726084568,26.7516161506131,24.2776953423726));
#52713=CARTESIAN_POINT('Ctrl Pts',(-24.0774731362469,26.7324184848717,24.2851622028118));
#52714=CARTESIAN_POINT('Ctrl Pts',(-24.3545482966431,26.6745710077587,24.3009834459309));
#52715=CARTESIAN_POINT('Ctrl Pts',(-24.4979148720412,26.6341120261508,24.3093308043312));
#52716=CARTESIAN_POINT('Ctrl Pts',(-24.7326848571957,26.5499352669083,24.3237800651477));
#52717=CARTESIAN_POINT('Ctrl Pts',(-24.8257532540196,26.5115592580394,24.3297234804835));
#52718=CARTESIAN_POINT('Ctrl Pts',(-24.9275987789843,26.4638714622227,24.3365359669732));
#52719=CARTESIAN_POINT('Ctrl Pts',(-24.9383016191099,26.4587878473393,24.3372557592595));
#52720=CARTESIAN_POINT('Ctrl Pts',(-24.9547161777229,26.4508800543719,24.3383657515743));
#52721=CARTESIAN_POINT('Ctrl Pts',(-24.9604480375965,26.4480977298627,24.3387544987821));
#52722=CARTESIAN_POINT('Ctrl Pts',(-24.9710873564993,26.4428942150551,24.339478228975));
#52723=CARTESIAN_POINT('Ctrl Pts',(-24.9759969805754,26.4404774837691,24.3398130555789));
#52724=CARTESIAN_POINT('Ctrl Pts',(-24.9840841354077,26.43647101244,24.3403660025021));
#52725=CARTESIAN_POINT('Ctrl Pts',(-24.9872652483703,26.4348884945769,24.3405838694409));
#52726=CARTESIAN_POINT('Ctrl Pts',(-24.9934794996717,26.4317842419193,24.3410101823424));
#52727=CARTESIAN_POINT('Ctrl Pts',(-24.9965128651859,26.430262970175,24.3412186118303));
#52728=CARTESIAN_POINT('Ctrl Pts',(-25.0035018748681,26.4267440659708,24.3416996143388));
#52729=CARTESIAN_POINT('Ctrl Pts',(-25.0074558061545,26.4247430633865,24.3419723057027));
#52730=CARTESIAN_POINT('Ctrl Pts',(-25.0197486811314,26.4184900126817,24.3428218977587));
#52731=CARTESIAN_POINT('Ctrl Pts',(-25.0280731794824,26.4142098132466,24.3433997906087));
#52732=CARTESIAN_POINT('Ctrl Pts',(-25.0985592178828,26.3775789356495,24.3483149972469));
#52733=CARTESIAN_POINT('Ctrl Pts',(-25.1596647473001,26.3432472084175,24.3527224178789));
#52734=CARTESIAN_POINT('Ctrl Pts',(-25.2262875569993,26.3029031261272,24.3576990825772));
#52735=CARTESIAN_POINT('Ctrl Pts',(-25.2329611246031,26.2988286159157,24.3581995407796));
#52736=CARTESIAN_POINT('Ctrl Pts',(-25.3392779846162,26.2333851106255,24.3662035614789));
#52737=CARTESIAN_POINT('Ctrl Pts',(-25.4355109429511,26.1666638742353,24.3738920895116));
#52738=CARTESIAN_POINT('Ctrl Pts',(-25.5893679031738,26.047088034922,24.3869034538945));
#52739=CARTESIAN_POINT('Ctrl Pts',(-25.6490874218692,25.9971016075127,24.392151655686));
#52740=CARTESIAN_POINT('Ctrl Pts',(-25.8277435836705,25.8362060101559,24.4084118474589));
#52741=CARTESIAN_POINT('Ctrl Pts',(-25.9401502971111,25.7184182410306,24.4194691482687));
#52742=CARTESIAN_POINT('Ctrl Pts',(-26.0865598898561,25.5397111010809,24.4346449286161));
#52743=CARTESIAN_POINT('Ctrl Pts',(-26.1282346035031,25.4854038087505,24.4390677021774));
#52744=CARTESIAN_POINT('Ctrl Pts',(-26.1745655922208,25.4208726081644,24.4440705412725));
#52745=CARTESIAN_POINT('Ctrl Pts',(-26.1809339011975,25.4119061113493,24.4447601826025));
#52746=CARTESIAN_POINT('Ctrl Pts',(-26.1891534818622,25.4002066471059,24.4456527190623));
#52747=CARTESIAN_POINT('Ctrl Pts',(-26.1910465301905,25.3975033299523,24.4458584473119));
#52748=CARTESIAN_POINT('Ctrl Pts',(-26.1941091300579,25.3931155366388,24.4461915448068));
#52749=CARTESIAN_POINT('Ctrl Pts',(-26.1952812260625,25.391432852502,24.4463190892971));
#52750=CARTESIAN_POINT('Ctrl Pts',(-26.1975285744576,25.3881999398796,24.4465637609153));
#52751=CARTESIAN_POINT('Ctrl Pts',(-26.1986040684866,25.3866498904999,24.4466809044325));
#52752=CARTESIAN_POINT('Ctrl Pts',(-26.2010742788195,25.3830830312749,24.4469500854416));
#52753=CARTESIAN_POINT('Ctrl Pts',(-26.2024680583072,25.3810655684935,24.4471020581985));
#52754=CARTESIAN_POINT('Ctrl Pts',(-26.206179773632,25.375679814866,24.4475070202332));
#52755=CARTESIAN_POINT('Ctrl Pts',(-26.2084936138016,25.372308686276,24.4477597296647));
#52756=CARTESIAN_POINT('Ctrl Pts',(-26.2241744231407,25.3493692246748,24.4494741764484));
#52757=CARTESIAN_POINT('Ctrl Pts',(-26.2373320724234,25.3296577068003,24.4509218975529));
#52758=CARTESIAN_POINT('Ctrl Pts',(-26.4264526356753,25.0394532647605,24.4718944784099));
#52759=CARTESIAN_POINT('Ctrl Pts',(-26.5610622265451,24.7441320491174,24.48908181635));
#52760=CARTESIAN_POINT('Ctrl Pts',(-26.6777387859486,24.3348033696304,24.5132784037033));
#52761=CARTESIAN_POINT('Ctrl Pts',(-26.70117466175,24.2346335213793,24.5192113911714));
#52762=CARTESIAN_POINT('Ctrl Pts',(-26.7316214122632,24.0691832416836,24.5291575731653));
#52763=CARTESIAN_POINT('Ctrl Pts',(-26.7414986148808,24.0045041589202,24.5330811276687));
#52764=CARTESIAN_POINT('Ctrl Pts',(-26.7504213975063,23.9311832561042,24.5375832887968));
#52765=CARTESIAN_POINT('Ctrl Pts',(-26.7514093305785,23.9227899570974,24.5380994598241));
#52766=CARTESIAN_POINT('Ctrl Pts',(-26.752842333348,23.9101886776667,24.5388756343341));
#52767=CARTESIAN_POINT('Ctrl Pts',(-26.7533121538779,23.9059835020947,24.5391348555624));
#52768=CARTESIAN_POINT('Ctrl Pts',(-26.7541054000862,23.8987544806794,24.5395808314792));
#52769=CARTESIAN_POINT('Ctrl Pts',(-26.7544328306971,23.8957310724557,24.5397674594396));
#52770=CARTESIAN_POINT('Ctrl Pts',(-26.7550978600462,23.8895080918584,24.5401518106526));
#52771=CARTESIAN_POINT('Ctrl Pts',(-26.7554349478226,23.8863084689684,24.5403495498385));
#52772=CARTESIAN_POINT('Ctrl Pts',(-26.7562341647953,23.8786117379118,24.540825505401));
#52773=CARTESIAN_POINT('Ctrl Pts',(-26.7566916228442,23.8741141603431,24.5411038689284));
#52774=CARTESIAN_POINT('Ctrl Pts',(-26.7580641451004,23.8603319682164,24.5419576162046));
#52775=CARTESIAN_POINT('Ctrl Pts',(-26.7589483505287,23.8510443921432,24.5425339721548));
#52776=CARTESIAN_POINT('Ctrl Pts',(-26.7686540843315,23.7441803514128,24.5491777037408));
#52777=CARTESIAN_POINT('Ctrl Pts',(-26.7730610902647,23.6462638720254,24.5553836380815));
#52778=CARTESIAN_POINT('Ctrl Pts',(-26.7729532790423,23.4677077078081,24.5669332623744));
#52779=CARTESIAN_POINT('Ctrl Pts',(-26.7698810632503,23.3871442905677,24.5722302431843));
#52780=CARTESIAN_POINT('Ctrl Pts',(-26.7397931034448,22.9900111221567,24.598718681482));
#52781=CARTESIAN_POINT('Ctrl Pts',(-26.6690921232823,22.6785448539725,24.6208881486241));
#52782=CARTESIAN_POINT('Ctrl Pts',(-26.5480385604194,22.3671780095951,24.6420336191901));
#52783=CARTESIAN_POINT('Ctrl Pts',(-26.541980549888,22.3519412653005,24.6430651416269));
#52784=CARTESIAN_POINT('Ctrl Pts',(-26.5344503637869,22.3334148966652,24.6443148333827));
#52785=CARTESIAN_POINT('Ctrl Pts',(-26.5330887635058,22.330081008672,24.6445395399804));
#52786=CARTESIAN_POINT('Ctrl Pts',(-26.5308370263427,22.3245939082232,24.644909069626));
#52787=CARTESIAN_POINT('Ctrl Pts',(-26.5299501425287,22.3224393785286,24.64505408917));
#52788=CARTESIAN_POINT('Ctrl Pts',(-26.5283482354139,22.3185597822403,24.6453150791071));
#52789=CARTESIAN_POINT('Ctrl Pts',(-26.5276340509093,22.3168343792954,24.6454311002531));
#52790=CARTESIAN_POINT('Ctrl Pts',(-26.526096627323,22.3131292241444,24.6456801359081));
#52791=CARTESIAN_POINT('Ctrl Pts',(-26.525272914391,22.3111496779428,24.6458131206096));
#52792=CARTESIAN_POINT('Ctrl Pts',(-26.5230154365776,22.3057397366306,24.6461763774884));
#52793=CARTESIAN_POINT('Ctrl Pts',(-26.5215777042952,22.3023109846952,24.6464064073956));
#52794=CARTESIAN_POINT('Ctrl Pts',(-26.5141336189494,22.2846438759967,24.6475906857598));
#52795=CARTESIAN_POINT('Ctrl Pts',(-26.5080307117073,22.2704460505562,24.6485391158548));
#52796=CARTESIAN_POINT('Ctrl Pts',(-26.4694082632743,22.1823467520432,24.6544069993));
#52797=CARTESIAN_POINT('Ctrl Pts',(-26.4342202860548,22.1096384905802,24.6591740889681));
#52798=CARTESIAN_POINT('Ctrl Pts',(-26.3220131426054,21.8984178762582,24.6730164145676));
#52799=CARTESIAN_POINT('Ctrl Pts',(-26.2374716622895,21.7641745519564,24.6818136922495));
#52800=CARTESIAN_POINT('Ctrl Pts',(-26.1166529820714,21.600448800247,24.6931880214801));
#52801=CARTESIAN_POINT('Ctrl Pts',(-26.0891552004595,21.5647755019798,24.6957083210066));
#52802=CARTESIAN_POINT('Ctrl Pts',(-25.9297076738589,21.3666526189152,24.7100007969063));
#52803=CARTESIAN_POINT('Ctrl Pts',(-25.7829501076783,21.2168093748268,24.7220024714878));
#52804=CARTESIAN_POINT('Ctrl Pts',(-25.6128848020216,21.0739991900047,24.7354949374918));
#52805=CARTESIAN_POINT('Ctrl Pts',(-25.6030007251963,21.0657994044616,24.7362775821494));
#52806=CARTESIAN_POINT('Ctrl Pts',(-25.5894661413546,21.0547070794872,24.7373473163125));
#52807=CARTESIAN_POINT('Ctrl Pts',(-25.5858578912978,21.0517629740937,24.7376323130007));
#52808=CARTESIAN_POINT('Ctrl Pts',(-25.5797172095469,21.0467746956253,24.7381170185827));
#52809=CARTESIAN_POINT('Ctrl Pts',(-25.5771880316916,21.0447265124571,24.7383165651992));
#52810=CARTESIAN_POINT('Ctrl Pts',(-25.5722990961098,21.0407795935046,24.7387021196412));
#52811=CARTESIAN_POINT('Ctrl Pts',(-25.5699397551325,21.0388803459056,24.738888106507));
#52812=CARTESIAN_POINT('Ctrl Pts',(-25.564348694931,21.0343925689252,24.739328669771));
#52813=CARTESIAN_POINT('Ctrl Pts',(-25.5611146633544,21.0318069408129,24.7395833623625));
#52814=CARTESIAN_POINT('Ctrl Pts',(-25.5516084950091,21.0242366851615,24.7403316004087));
#52815=CARTESIAN_POINT('Ctrl Pts',(-25.5453227772385,21.0192692322004,24.7408258324094));
#52816=CARTESIAN_POINT('Ctrl Pts',(-25.4980521271458,20.982197873776,24.7445388269298));
#52817=CARTESIAN_POINT('Ctrl Pts',(-25.456315207615,20.9510694767509,24.7477960612853));
#52818=CARTESIAN_POINT('Ctrl Pts',(-25.3154040511981,20.8511940906729,24.7587331851646));
#52819=CARTESIAN_POINT('Ctrl Pts',(-25.2131339680768,20.7870124252903,24.7665804253408));
#52820=CARTESIAN_POINT('Ctrl Pts',(-24.83639151254,20.5790801916629,24.7951218745607));
#52821=CARTESIAN_POINT('Ctrl Pts',(-24.5451386335911,20.4693099927126,24.8167011456358));
#52822=CARTESIAN_POINT('Ctrl Pts',(-24.2360699690346,20.4013133005574,24.8369786526742));
#52823=CARTESIAN_POINT('Ctrl Pts',(-24.2294215172514,20.3998726610214,24.8374135655674));
#52824=CARTESIAN_POINT('Ctrl Pts',(-24.197400640427,20.3930401988073,24.8395019080729));
#52825=CARTESIAN_POINT('Ctrl Pts',(-24.1719673667614,20.3879335791155,24.8411415318508));
#52826=CARTESIAN_POINT('Ctrl Pts',(-24.1423364936593,20.3823554575764,24.8430274432683));
#52827=CARTESIAN_POINT('Ctrl Pts',(-24.1381971945408,20.3815846153403,24.8432903465017));
#52828=CARTESIAN_POINT('Ctrl Pts',(-24.1316096872305,20.3803712074859,24.8437078573127));
#52829=CARTESIAN_POINT('Ctrl Pts',(-24.1291624747587,20.3799233642765,24.8438627648723));
#52830=CARTESIAN_POINT('Ctrl Pts',(-24.1248529395932,20.3791398697725,24.8441352108989));
#52831=CARTESIAN_POINT('Ctrl Pts',(-24.1229908379986,20.3788030246195,24.8442528180959));
#52832=CARTESIAN_POINT('Ctrl Pts',(-24.1191663189272,20.3781146658715,24.8444941337254));
#52833=CARTESIAN_POINT('Ctrl Pts',(-24.1172038756575,20.3777633338055,24.8446178314743));
#52834=CARTESIAN_POINT('Ctrl Pts',(-24.1121679294303,20.3768665809872,24.8449349382581));
#52835=CARTESIAN_POINT('Ctrl Pts',(-24.1090939486703,20.3763238026226,24.8451281954669));
#52836=CARTESIAN_POINT('Ctrl Pts',(-24.1024078575175,20.375153241913,24.845547882996));
#52837=CARTESIAN_POINT('Ctrl Pts',(-24.0987954491213,20.3745271544209,24.8457742171639));
#52838=CARTESIAN_POINT('Ctrl Pts',(-24.0883541735169,20.3727358635519,24.8464272258668));
#52839=CARTESIAN_POINT('Ctrl Pts',(-24.0815225557165,20.3715865038012,24.846853018013));
#52840=CARTESIAN_POINT('Ctrl Pts',(-24.0127774721639,20.360248563938,24.8511234306534));
#52841=CARTESIAN_POINT('Ctrl Pts',(-23.9505777715584,20.3518473693978,24.8548711967023));
#52842=CARTESIAN_POINT('Ctrl Pts',(-23.8454976721986,20.3407683302316,24.8610676541603));
#52843=CARTESIAN_POINT('Ctrl Pts',(-23.8027404482539,20.3371218685373,24.8635516411557));
#52844=CARTESIAN_POINT('Ctrl Pts',(-23.3754786246961,20.3092655974738,24.8881110827195));
#52845=CARTESIAN_POINT('Ctrl Pts',(-22.9896769918236,20.3533274079918,24.9086083127863));
#52846=CARTESIAN_POINT('Ctrl Pts',(-22.6016145333458,20.4702196020796,24.9331236884112));
#52847=CARTESIAN_POINT('Ctrl Pts',(-22.5825346962012,20.4761609484275,24.9343381554212));
#52848=CARTESIAN_POINT('Ctrl Pts',(-22.5576050008768,20.4841789937812,24.9359373636615));
#52849=CARTESIAN_POINT('Ctrl Pts',(-22.5517038574818,20.4860957790613,24.9363168281429));
#52850=CARTESIAN_POINT('Ctrl Pts',(-22.5426041594643,20.4890805842725,24.9369033951151));
#52851=CARTESIAN_POINT('Ctrl Pts',(-22.5394016615432,20.4901366103742,24.9371101010624));
#52852=CARTESIAN_POINT('Ctrl Pts',(-22.5330268401287,20.4922498115842,24.9375221113758));
#52853=CARTESIAN_POINT('Ctrl Pts',(-22.5298544926599,20.4933069015623,24.9377274127124));
#52854=CARTESIAN_POINT('Ctrl Pts',(-22.5228246993689,20.4956615320021,24.9381829530888));
#52855=CARTESIAN_POINT('Ctrl Pts',(-22.5189680593784,20.4969614445303,24.9384332704571));
#52856=CARTESIAN_POINT('Ctrl Pts',(-22.5078445224066,20.500734204556,24.9391564159176));
#52857=CARTESIAN_POINT('Ctrl Pts',(-22.5005840217141,20.5032257016678,24.939629862212));
#52858=CARTESIAN_POINT('Ctrl Pts',(-22.4516090163294,20.5202276730268,24.9428332612695));
#52859=CARTESIAN_POINT('Ctrl Pts',(-22.4101894378261,20.5355677974494,24.9455907277039));
#52860=CARTESIAN_POINT('Ctrl Pts',(-22.3117588115538,20.574341067129,24.9522642590641));
#52861=CARTESIAN_POINT('Ctrl Pts',(-22.2550809416906,20.598567340342,24.9562060089334));
#52862=CARTESIAN_POINT('Ctrl Pts',(-22.0789744392539,20.6798908879159,24.9687713324372));
#52863=CARTESIAN_POINT('Ctrl Pts',(-21.9623576921053,20.7427235660855,24.9775699975659));
#52864=CARTESIAN_POINT('Ctrl Pts',(-21.6451297509722,20.9397441156922,25.0027143190638));
#52865=CARTESIAN_POINT('Ctrl Pts',(-21.4552298247767,21.0895334345474,25.0192873671481));
#52866=CARTESIAN_POINT('Ctrl Pts',(-21.2586248342316,21.2840189178179,25.0370468952579));
#52867=CARTESIAN_POINT('Ctrl Pts',(-21.2338532677246,21.3093449020208,25.0392957069507));
#52868=CARTESIAN_POINT('Ctrl Pts',(-21.2063197868229,21.3384391810442,25.0418027066979));
#52869=CARTESIAN_POINT('Ctrl Pts',(-21.2031437277352,21.3418098057879,25.0420920100669));
#52870=CARTESIAN_POINT('Ctrl Pts',(-21.1983504121396,21.3469187803925,25.0425287843651));
#52871=CARTESIAN_POINT('Ctrl Pts',(-21.1967278098213,21.3486520722073,25.0426766657259));
#52872=CARTESIAN_POINT('Ctrl Pts',(-21.193910474493,21.3516682724116,25.0429334781585));
#52873=CARTESIAN_POINT('Ctrl Pts',(-21.1927148730194,21.3529503622909,25.0430424765985));
#52874=CARTESIAN_POINT('Ctrl Pts',(-21.1902419150939,21.3556065529986,25.043267954839));
#52875=CARTESIAN_POINT('Ctrl Pts',(-21.1889647132758,21.3569807927435,25.043384422373));
#52876=CARTESIAN_POINT('Ctrl Pts',(-21.1859312665289,21.3602504324938,25.0436610799906));
#52877=CARTESIAN_POINT('Ctrl Pts',(-21.1841760947002,21.3621468363885,25.0438211868869));
#52878=CARTESIAN_POINT('Ctrl Pts',(-21.1804560861729,21.3661758897255,25.0441605975087));
#52879=CARTESIAN_POINT('Ctrl Pts',(-21.1784918414152,21.3683090861846,25.0443398559366));
#52880=CARTESIAN_POINT('Ctrl Pts',(-21.1731574306548,21.3741180431605,25.0448268029681));
#52881=CARTESIAN_POINT('Ctrl Pts',(-21.1697928957499,21.3777989984767,25.04513406747));
#52882=CARTESIAN_POINT('Ctrl Pts',(-21.0693595185165,21.4881911721281,25.0543107079177));
#52883=CARTESIAN_POINT('Ctrl Pts',(-20.9795412084919,21.6013085658299,25.062649323268));
#52884=CARTESIAN_POINT('Ctrl Pts',(-20.6988727174088,22.0081102138774,25.0906341108799));
#52885=CARTESIAN_POINT('Ctrl Pts',(-20.5484005595743,22.3265478018212,25.1095574545639));
#52886=CARTESIAN_POINT('Ctrl Pts',(-20.446453899504,22.6825165602709,25.1319505526884));
#52887=CARTESIAN_POINT('Ctrl Pts',(-20.4410367181624,22.7021318677329,25.1331871081912));
#52888=CARTESIAN_POINT('Ctrl Pts',(-20.4341993272694,22.7278359454309,25.1348113212676));
#52889=CARTESIAN_POINT('Ctrl Pts',(-20.432610472652,22.7338796971452,25.1351934939566));
#52890=CARTESIAN_POINT('Ctrl Pts',(-20.4301890779167,22.7432004648039,25.1357833221574));
#52891=CARTESIAN_POINT('Ctrl Pts',(-20.4293440935351,22.7464742570694,25.1359905739199));
#52892=CARTESIAN_POINT('Ctrl Pts',(-20.4276738500891,22.7529877598102,25.1364030867017));
#52893=CARTESIAN_POINT('Ctrl Pts',(-20.4268484771296,22.7562274369412,25.1366083437398));
#52894=CARTESIAN_POINT('Ctrl Pts',(-20.4250330891775,22.7633996587312,25.1370629399854));
#52895=CARTESIAN_POINT('Ctrl Pts',(-20.4240454539403,22.7673327948525,25.1373123558582));
#52896=CARTESIAN_POINT('Ctrl Pts',(-20.4212263519589,22.778649909517,25.1380303766606));
#52897=CARTESIAN_POINT('Ctrl Pts',(-20.4194136137085,22.7860384857256,25.1384995862627));
#52898=CARTESIAN_POINT('Ctrl Pts',(-20.4075895282158,22.8349807334184,25.1416106249113));
#52899=CARTESIAN_POINT('Ctrl Pts',(-20.3983799463952,22.8767219673827,25.1442781858845));
#52900=CARTESIAN_POINT('Ctrl Pts',(-20.3738615614906,22.999397295641,25.1521642389251));
#52901=CARTESIAN_POINT('Ctrl Pts',(-20.3608228523623,23.0807448471439,25.1574528943659));
#52902=CARTESIAN_POINT('Ctrl Pts',(-20.3149321040827,23.4593854792597,25.1823434440813));
#52903=CARTESIAN_POINT('Ctrl Pts',(-20.3204521299649,23.7597799160756,25.2030439281942));
#52904=CARTESIAN_POINT('Ctrl Pts',(-20.3812016216365,24.1428099604202,25.2286830214828));
#52905=CARTESIAN_POINT('Ctrl Pts',(-20.39873887127,24.2299385119705,25.2344477288169));
#52906=CARTESIAN_POINT('Ctrl Pts',(-20.4213760974434,24.3224511558062,25.2404183219073));
#52907=CARTESIAN_POINT('Ctrl Pts',(-20.4229145198483,24.328658221047,25.2408181769383));
#52908=CARTESIAN_POINT('Ctrl Pts',(-20.4250739235547,24.3372610158356,25.241371300147));
#52909=CARTESIAN_POINT('Ctrl Pts',(-20.4256791911111,24.3396606177319,25.241525469492));
#52910=CARTESIAN_POINT('Ctrl Pts',(-20.4267243647189,24.3437842060544,25.2417902009331));
#52911=CARTESIAN_POINT('Ctrl Pts',(-20.4271629342986,24.3455085249292,25.2419008407081));
#52912=CARTESIAN_POINT('Ctrl Pts',(-20.4280454516656,24.3489663189318,25.2421225856057));
#52913=CARTESIAN_POINT('Ctrl Pts',(-20.4284894143094,24.3506997838299,25.2422336891917));
#52914=CARTESIAN_POINT('Ctrl Pts',(-20.4295424603684,24.3547972306367,25.2424961638094));
#52915=CARTESIAN_POINT('Ctrl Pts',(-20.430152787981,24.357160897772,25.2426474621104));
#52916=CARTESIAN_POINT('Ctrl Pts',(-20.4320677089244,24.3645423162451,25.2431195978627));
#52917=CARTESIAN_POINT('Ctrl Pts',(-20.4333817336143,24.3695576464969,25.2434398884316));
#52918=CARTESIAN_POINT('Ctrl Pts',(-20.4364583153547,24.3811857269735,25.2441813617453));
#52919=CARTESIAN_POINT('Ctrl Pts',(-20.4382298518671,24.3877961060512,25.2446020338253));
#52920=CARTESIAN_POINT('Ctrl Pts',(-20.4442667959811,24.4100389803399,25.2460148400851));
#52921=CARTESIAN_POINT('Ctrl Pts',(-20.448629122822,24.4256452332248,25.2470016274361));
#52922=CARTESIAN_POINT('Ctrl Pts',(-20.4673307877551,24.4906552957092,25.2510960504461));
#52923=CARTESIAN_POINT('Ctrl Pts',(-20.4827350188909,24.5397477507378,25.2541488470215));
#52924=CARTESIAN_POINT('Ctrl Pts',(-20.5460188343804,24.7257188774601,25.2656371221783));
#52925=CARTESIAN_POINT('Ctrl Pts',(-20.6019430438989,24.8596871939321,25.2737582007767));
#52926=CARTESIAN_POINT('Ctrl Pts',(-20.7918160437981,25.24011510201,25.2975249315984));
#52927=CARTESIAN_POINT('Ctrl Pts',(-20.9490563559416,25.4733646062996,25.3131401889811));
#52928=CARTESIAN_POINT('Ctrl Pts',(-21.1464787723451,25.6969520974813,25.3312020212581));
#52929=CARTESIAN_POINT('Ctrl Pts',(-21.1586125674031,25.7104621446849,25.3323063414239));
#52930=CARTESIAN_POINT('Ctrl Pts',(-21.1748877385455,25.7282780893167,25.3337802703979));
#52931=CARTESIAN_POINT('Ctrl Pts',(-21.1789280054581,25.7326762349881,25.3341455797796));
#52932=CARTESIAN_POINT('Ctrl Pts',(-21.1852368393966,25.7395056909266,25.3347151029217));
#52933=CARTESIAN_POINT('Ctrl Pts',(-21.1874969981602,25.7419447793979,25.3349189568964));
#52934=CARTESIAN_POINT('Ctrl Pts',(-21.1920194678573,25.7468101530787,25.3353265035709));
#52935=CARTESIAN_POINT('Ctrl Pts',(-21.1942817582284,25.7492364520269,25.3355301952603));
#52936=CARTESIAN_POINT('Ctrl Pts',(-21.199374551669,25.7546815758282,25.3359883452474));
#52937=CARTESIAN_POINT('Ctrl Pts',(-21.2022071272738,25.7576984463462,25.3362428926513));
#52938=CARTESIAN_POINT('Ctrl Pts',(-21.2105329061001,25.7665317655877,25.3369902919019));
#52939=CARTESIAN_POINT('Ctrl Pts',(-21.2160419370033,25.7723331933175,25.3374838279577));
#52940=CARTESIAN_POINT('Ctrl Pts',(-21.257360581219,25.8155216518161,25.3411780548802));
#52941=CARTESIAN_POINT('Ctrl Pts',(-21.2940430476527,25.8520596355479,25.3444167800098));
#52942=CARTESIAN_POINT('Ctrl Pts',(-21.4183058517872,25.9700079021186,25.3552644042781));
#52943=CARTESIAN_POINT('Ctrl Pts',(-21.5095273206934,26.0474204597432,25.363037371445));
#52944=CARTESIAN_POINT('Ctrl Pts',(-21.7077729659232,26.1975265358039,25.3795235101272));
#52945=CARTESIAN_POINT('Ctrl Pts',(-21.8153028012303,26.2692112433931,25.3882482032679));
#52946=CARTESIAN_POINT('Ctrl Pts',(-21.9755324628609,26.362645105302,25.4008038841439));
#52947=CARTESIAN_POINT('Ctrl Pts',(-22.0249500916317,26.3897496042714,25.4046182645467));
#52948=CARTESIAN_POINT('Ctrl Pts',(-22.0750361607755,26.4155368494319,25.4084140214669));
#52949=CARTESIAN_POINT('Origin',(-23.5502525316942,23.5502525316942,-77.3107734492734));
#52950=CARTESIAN_POINT('',(-22.0750359502314,26.4155367410314,26.9066135500179));
#52951=CARTESIAN_POINT('',(-22.0750360239718,26.4155367789973,26.65912344949));
#52952=CARTESIAN_POINT('',(-22.0750360153461,26.4155367745563,-77.3107734492734));
#52953=CARTESIAN_POINT('',(-26.7730012737579,23.5530999914162,26.0607734492728));
#52954=CARTESIAN_POINT('Ctrl Pts',(-22.0750359502314,26.4155367410314,26.9066135500179));
#52955=CARTESIAN_POINT('Ctrl Pts',(-21.9929580785884,26.3732782324952,26.9007492253846));
#52956=CARTESIAN_POINT('Ctrl Pts',(-21.9127240473899,26.3275074705045,26.8947643953227));
#52957=CARTESIAN_POINT('Ctrl Pts',(-21.6109491453685,26.1377214829904,26.8712772276802));
#52958=CARTESIAN_POINT('Ctrl Pts',(-21.4055080510349,25.9701579434784,26.8530612011559));
#52959=CARTESIAN_POINT('Ctrl Pts',(-21.2053313937181,25.7611577773525,26.8338699128938));
#52960=CARTESIAN_POINT('Ctrl Pts',(-21.1880535021463,25.7426879249033,26.8322008762093));
#52961=CARTESIAN_POINT('Ctrl Pts',(-21.1513291836319,25.7024919116327,26.8286292740379));
#52962=CARTESIAN_POINT('Ctrl Pts',(-21.1319562669122,25.6807010448331,26.8267301350214));
#52963=CARTESIAN_POINT('Ctrl Pts',(-21.1113016857495,25.6568237177462,26.8246915435628));
#52964=CARTESIAN_POINT('Ctrl Pts',(-21.1097243110865,25.6549960779077,26.8245357691453));
#52965=CARTESIAN_POINT('Ctrl Pts',(-21.0806070557029,25.6211823564755,26.8216586648387));
#52966=CARTESIAN_POINT('Ctrl Pts',(-21.0536944342395,25.5886580881064,26.8189726210674));
#52967=CARTESIAN_POINT('Ctrl Pts',(-21.0243990343653,25.5518032684836,26.8160271449043));
#52968=CARTESIAN_POINT('Ctrl Pts',(-21.021379674926,25.5479870778619,26.8157233030136));
#52969=CARTESIAN_POINT('Ctrl Pts',(-21.0168917286336,25.5422882504382,26.8152713003195));
#52970=CARTESIAN_POINT('Ctrl Pts',(-21.0154165894096,25.5404108191244,26.8151226711923));
#52971=CARTESIAN_POINT('Ctrl Pts',(-21.0127881859765,25.5370579483385,26.8148577378918));
#52972=CARTESIAN_POINT('Ctrl Pts',(-21.0116341225899,25.5355831445693,26.8147413761529));
#52973=CARTESIAN_POINT('Ctrl Pts',(-21.009184919501,25.532447625034,26.8144943514059));
#52974=CARTESIAN_POINT('Ctrl Pts',(-21.0078901254244,25.5307866498161,26.8143637133598));
#52975=CARTESIAN_POINT('Ctrl Pts',(-21.0044622465206,25.5263804305846,26.8140177321108));
#52976=CARTESIAN_POINT('Ctrl Pts',(-21.0023319665997,25.5236329925017,26.8138025899507));
#52977=CARTESIAN_POINT('Ctrl Pts',(-20.9924273492387,25.5108161575393,26.8128016650482));
#52978=CARTESIAN_POINT('Ctrl Pts',(-20.9847080900109,25.5007040500474,26.812019760336));
#52979=CARTESIAN_POINT('Ctrl Pts',(-20.7995041246043,25.2550878707824,26.7932083176412));
#52980=CARTESIAN_POINT('Ctrl Pts',(-20.6550822945767,24.9963291544905,26.7772938720883));
#52981=CARTESIAN_POINT('Ctrl Pts',(-20.4743189284497,24.5329555553363,26.749302234164));
#52982=CARTESIAN_POINT('Ctrl Pts',(-20.418703522984,24.3379421294129,26.7376682853775));
#52983=CARTESIAN_POINT('Ctrl Pts',(-20.3794399493201,24.1266409828942,26.7246084225434));
#52984=CARTESIAN_POINT('Ctrl Pts',(-20.3772123934014,24.1142492984843,26.7238410681121));
#52985=CARTESIAN_POINT('Ctrl Pts',(-20.3742671200533,24.0972950841248,26.7227890822467));
#52986=CARTESIAN_POINT('Ctrl Pts',(-20.3734864933887,24.0927434778248,26.7225064551499));
#52987=CARTESIAN_POINT('Ctrl Pts',(-20.3721742213014,24.0849920356542,26.7220247812454));
#52988=CARTESIAN_POINT('Ctrl Pts',(-20.3716376170277,24.081793036481,26.7218258924725));
#52989=CARTESIAN_POINT('Ctrl Pts',(-20.3706088181759,24.0756025188826,26.7214408125975));
#52990=CARTESIAN_POINT('Ctrl Pts',(-20.3701160133923,24.0726111047257,26.7212546411682));
#52991=CARTESIAN_POINT('Ctrl Pts',(-20.3689562580605,24.0655087076917,26.7208124033243));
#52992=CARTESIAN_POINT('Ctrl Pts',(-20.3682930550723,24.0613971261251,26.7205562180498));
#52993=CARTESIAN_POINT('Ctrl Pts',(-20.3663590197998,24.0492572767993,26.7197992872649));
#52994=CARTESIAN_POINT('Ctrl Pts',(-20.3651105952358,24.0412255181145,26.7192978306633));
#52995=CARTESIAN_POINT('Ctrl Pts',(-20.3557603508492,23.9795336910117,26.7154408996367));
#52996=CARTESIAN_POINT('Ctrl Pts',(-20.3489851130133,23.9256842046718,26.7120435728685));
#52997=CARTESIAN_POINT('Ctrl Pts',(-20.3306847416764,23.7431196538725,26.7004123636756));
#52998=CARTESIAN_POINT('Ctrl Pts',(-20.3255423204574,23.6139040441732,26.691984346246));
#52999=CARTESIAN_POINT('Ctrl Pts',(-20.3322283547432,23.2850599754964,26.6701001880548));
#53000=CARTESIAN_POINT('Ctrl Pts',(-20.3548422769434,23.0861911286024,26.6564362419457));
#53001=CARTESIAN_POINT('Ctrl Pts',(-20.4154147502456,22.7964764885113,26.636607079519));
#53002=CARTESIAN_POINT('Ctrl Pts',(-20.4393320327008,22.7031615121302,26.6302395293287));
#53003=CARTESIAN_POINT('Ctrl Pts',(-20.4774241329454,22.5781271704303,26.621851422128));
#53004=CARTESIAN_POINT('Ctrl Pts',(-20.4879814775342,22.545365316744,26.6196674153321));
#53005=CARTESIAN_POINT('Ctrl Pts',(-20.5005403941846,22.5084298374257,26.6172259407769));
#53006=CARTESIAN_POINT('Ctrl Pts',(-20.5020279274436,22.5040855227381,26.6169391048877));
#53007=CARTESIAN_POINT('Ctrl Pts',(-20.5042953516082,22.4975094441835,26.6165054286955));
#53008=CARTESIAN_POINT('Ctrl Pts',(-20.5050684134697,22.4952753578083,26.6163581860571));
#53009=CARTESIAN_POINT('Ctrl Pts',(-20.5064181496661,22.4913885738573,26.6161021775316));
#53010=CARTESIAN_POINT('Ctrl Pts',(-20.5069937121586,22.489735495633,26.6159933452904));
#53011=CARTESIAN_POINT('Ctrl Pts',(-20.5082025576762,22.4862726473117,26.6157654710598));
#53012=CARTESIAN_POINT('Ctrl Pts',(-20.5088361087086,22.4844629742256,26.6156464457261));
#53013=CARTESIAN_POINT('Ctrl Pts',(-20.5101025638427,22.4808558012765,26.6154093154137));
#53014=CARTESIAN_POINT('Ctrl Pts',(-20.5107354488026,22.4790582930473,26.61529120914));
#53015=CARTESIAN_POINT('Ctrl Pts',(-20.5129530680002,22.4727776409226,26.6148787392868));
#53016=CARTESIAN_POINT('Ctrl Pts',(-20.5145461395474,22.4682974153582,26.6145848722831));
#53017=CARTESIAN_POINT('Ctrl Pts',(-20.5291066868773,22.4276338368715,26.6119208280811));
#53018=CARTESIAN_POINT('Ctrl Pts',(-20.5427112982238,22.391679702484,26.6095880784015));
#53019=CARTESIAN_POINT('Ctrl Pts',(-20.589402146365,22.2746553121679,26.6020436972514));
#53020=CARTESIAN_POINT('Ctrl Pts',(-20.6251508737185,22.1946839801035,26.5969646629299));
#53021=CARTESIAN_POINT('Ctrl Pts',(-20.7267077887733,21.9902843190817,26.5839413803056));
#53022=CARTESIAN_POINT('Ctrl Pts',(-20.7974836718896,21.8685354363971,26.5761371601335));
#53023=CARTESIAN_POINT('Ctrl Pts',(-21.0087951290877,21.5543201850005,26.5549485094532));
#53024=CARTESIAN_POINT('Ctrl Pts',(-21.1630395322912,21.3721934311609,26.5414497116441));
#53025=CARTESIAN_POINT('Ctrl Pts',(-21.3465977419816,21.1986064023514,26.5261187780233));
#53026=CARTESIAN_POINT('Ctrl Pts',(-21.3573545353437,21.1885725541662,26.5252230144161));
#53027=CARTESIAN_POINT('Ctrl Pts',(-21.3722104315065,21.1749040992886,26.5239893564097));
#53028=CARTESIAN_POINT('Ctrl Pts',(-21.3762507841995,21.1712056706959,26.5236541859428));
#53029=CARTESIAN_POINT('Ctrl Pts',(-21.3826859585977,21.1653451701098,26.5231208926016));
#53030=CARTESIAN_POINT('Ctrl Pts',(-21.3850746448399,21.1631763514479,26.5229230562298));
#53031=CARTESIAN_POINT('Ctrl Pts',(-21.3897184776807,21.1589726672003,26.5225386700682));
#53032=CARTESIAN_POINT('Ctrl Pts',(-21.391973253086,21.1569373948351,26.52235213776));
#53033=CARTESIAN_POINT('Ctrl Pts',(-21.3973578747523,21.1520907651917,26.5219069244765));
#53034=CARTESIAN_POINT('Ctrl Pts',(-21.4004903493642,21.1492823483394,26.5216481199777));
#53035=CARTESIAN_POINT('Ctrl Pts',(-21.4098439790663,21.1409293413111,26.5208759010017));
#53036=CARTESIAN_POINT('Ctrl Pts',(-21.4160811146663,21.1354027706262,26.5203617313163));
#53037=CARTESIAN_POINT('Ctrl Pts',(-21.4675926406325,21.0901151256205,26.5161213592833));
#53038=CARTESIAN_POINT('Ctrl Pts',(-21.5139499108582,21.0516090754381,26.5123433922128));
#53039=CARTESIAN_POINT('Ctrl Pts',(-21.6313654016923,20.9595178955684,26.5028571202663));
#53040=CARTESIAN_POINT('Ctrl Pts',(-21.7036120563247,20.9075360553845,26.4970904530061));
#53041=CARTESIAN_POINT('Ctrl Pts',(-21.9423581700751,20.750330919305,26.4782675546142));
#53042=CARTESIAN_POINT('Ctrl Pts',(-22.1163721542714,20.6573543243392,26.4648652542607));
#53043=CARTESIAN_POINT('Ctrl Pts',(-22.4463253771609,20.5181805077695,26.4406986617962));
#53044=CARTESIAN_POINT('Ctrl Pts',(-22.5994050352915,20.4667449448191,26.4299403539007));
#53045=CARTESIAN_POINT('Ctrl Pts',(-22.7648687209819,20.4246519273755,26.4192023010467));
#53046=CARTESIAN_POINT('Ctrl Pts',(-22.7740375066119,20.4223623309353,26.4186101397418));
#53047=CARTESIAN_POINT('Ctrl Pts',(-22.7863588439786,20.4193430049712,26.4178183351114));
#53048=CARTESIAN_POINT('Ctrl Pts',(-22.7895024959003,20.4185776740635,26.4176166606129));
#53049=CARTESIAN_POINT('Ctrl Pts',(-22.7944287538752,20.4173862181472,26.417301173751));
#53050=CARTESIAN_POINT('Ctrl Pts',(-22.7962105688713,20.416956880145,26.4171871749746));
#53051=CARTESIAN_POINT('Ctrl Pts',(-22.7996328374256,20.4161353542496,26.4169684379536));
#53052=CARTESIAN_POINT('Ctrl Pts',(-22.8012732219503,20.4157429367227,26.4168636870527));
#53053=CARTESIAN_POINT('Ctrl Pts',(-22.8046603373505,20.4149354718866,26.4166475907927));
#53054=CARTESIAN_POINT('Ctrl Pts',(-22.806407101814,20.4145205976362,26.4165362558449));
#53055=CARTESIAN_POINT('Ctrl Pts',(-22.8103506211426,20.4135874524147,26.4162851458211));
#53056=CARTESIAN_POINT('Ctrl Pts',(-22.8125475785152,20.4130700284056,26.4161454198842));
#53057=CARTESIAN_POINT('Ctrl Pts',(-22.8228763173456,20.4106488695705,26.4154893006147));
#53058=CARTESIAN_POINT('Ctrl Pts',(-22.8310150339363,20.4087744181468,26.4149745883705));
#53059=CARTESIAN_POINT('Ctrl Pts',(-22.9198829470903,20.3886704525339,26.4093783977253));
#53060=CARTESIAN_POINT('Ctrl Pts',(-23.0012865531326,20.373523688671,26.4044682024706));
#53061=CARTESIAN_POINT('Ctrl Pts',(-23.2164576959292,20.3420069567183,26.3918396630189));
#53062=CARTESIAN_POINT('Ctrl Pts',(-23.3508265510868,20.3308592929678,26.3843007720226));
#53063=CARTESIAN_POINT('Ctrl Pts',(-23.7633768062159,20.3225693458991,26.3612379940522));
#53064=CARTESIAN_POINT('Ctrl Pts',(-24.0407564939307,20.3529504402609,26.3457327227698));
#53065=CARTESIAN_POINT('Ctrl Pts',(-24.3282978166272,20.4227794657512,26.3278131684815));
#53066=CARTESIAN_POINT('Ctrl Pts',(-24.3457715376222,20.4271784476771,26.3267173110875));
#53067=CARTESIAN_POINT('Ctrl Pts',(-24.3689680703198,20.4332254428591,26.3252530622308));
#53068=CARTESIAN_POINT('Ctrl Pts',(-24.3747247589748,20.4347431750384,26.324888899305));
#53069=CARTESIAN_POINT('Ctrl Pts',(-24.3836864500191,20.4371324733262,26.3243207636741));
#53070=CARTESIAN_POINT('Ctrl Pts',(-24.3868943870748,20.4379930631215,26.3241171478555));
#53071=CARTESIAN_POINT('Ctrl Pts',(-24.393304109499,20.4397232186575,26.3237098136718));
#53072=CARTESIAN_POINT('Ctrl Pts',(-24.3965058939394,20.4405927726757,26.3235060958981));
#53073=CARTESIAN_POINT('Ctrl Pts',(-24.4037049024312,20.442559851299,26.3230474928176));
#53074=CARTESIAN_POINT('Ctrl Pts',(-24.4077013576639,20.4436601452545,26.3227925176064));
#53075=CARTESIAN_POINT('Ctrl Pts',(-24.4194375208071,20.4469156879891,26.3220426039857));
#53076=CARTESIAN_POINT('Ctrl Pts',(-24.4271712629328,20.4490921605225,26.3215469742951));
#53077=CARTESIAN_POINT('Ctrl Pts',(-24.484599635823,20.4654859695957,26.3178555970315));
#53078=CARTESIAN_POINT('Ctrl Pts',(-24.5339514967645,20.4808673981169,26.3146219455358));
#53079=CARTESIAN_POINT('Ctrl Pts',(-24.6960868671618,20.5357117892988,26.3037850313776));
#53080=CARTESIAN_POINT('Ctrl Pts',(-24.8070346801265,20.5802550226636,26.2960178664573));
#53081=CARTESIAN_POINT('Ctrl Pts',(-24.9894401422818,20.6655402183768,26.2826683935778));
#53082=CARTESIAN_POINT('Ctrl Pts',(-25.062283644121,20.7030456688475,26.2771728916489));
#53083=CARTESIAN_POINT('Ctrl Pts',(-25.2044124806302,20.7832181463539,26.2661606963856));
#53084=CARTESIAN_POINT('Ctrl Pts',(-25.2736720646164,20.8258169203984,26.2606483207847));
#53085=CARTESIAN_POINT('Ctrl Pts',(-25.4652580335461,20.9538853888959,26.24507414678));
#53086=CARTESIAN_POINT('Ctrl Pts',(-25.5833783245481,21.0453019704712,26.2350697739671));
#53087=CARTESIAN_POINT('Ctrl Pts',(-25.6978602503146,21.1473551116283,26.2252534180174));
#53088=CARTESIAN_POINT('Ctrl Pts',(-25.7009652328373,21.1501338258846,26.2249870881038));
#53089=CARTESIAN_POINT('Ctrl Pts',(-25.707790833634,21.1562660808022,26.2244014395974));
#53090=CARTESIAN_POINT('Ctrl Pts',(-25.7115090501165,21.1596222981147,26.2240822901335));
#53091=CARTESIAN_POINT('Ctrl Pts',(-25.7220667018086,21.1691968377854,26.2231757804333));
#53092=CARTESIAN_POINT('Ctrl Pts',(-25.7288872954969,21.1754359961367,26.2225897803661));
#53093=CARTESIAN_POINT('Ctrl Pts',(-25.746106009399,21.1913234798342,26.2211096994371));
#53094=CARTESIAN_POINT('Ctrl Pts',(-25.7564675882277,21.2010113969258,26.2202183767931));
#53095=CARTESIAN_POINT('Ctrl Pts',(-25.7694854376405,21.2133449779553,26.2190981025864));
#53096=CARTESIAN_POINT('Ctrl Pts',(-25.7722013046289,21.2159270924396,26.2188643586138));
#53097=CARTESIAN_POINT('Ctrl Pts',(-25.7764847900753,21.2200138710563,26.2184956651177));
#53098=CARTESIAN_POINT('Ctrl Pts',(-25.7780553904031,21.2215153832414,26.2183604718891));
#53099=CARTESIAN_POINT('Ctrl Pts',(-25.7809710768147,21.2243084626499,26.2181094870075));
#53100=CARTESIAN_POINT('Ctrl Pts',(-25.7823165521092,21.2255996008963,26.2179936635171));
#53101=CARTESIAN_POINT('Ctrl Pts',(-25.7849524194104,21.228133416825,26.2177667503164));
#53102=CARTESIAN_POINT('Ctrl Pts',(-25.7862428899571,21.2293759969358,26.2176556540014));
#53103=CARTESIAN_POINT('Ctrl Pts',(-25.7891471434974,21.232177141822,26.2174056167674));
#53104=CARTESIAN_POINT('Ctrl Pts',(-25.7907603385318,21.2337363190449,26.2172667237632));
#53105=CARTESIAN_POINT('Ctrl Pts',(-25.7948198819631,21.2376681361355,26.2169171819277));
#53106=CARTESIAN_POINT('Ctrl Pts',(-25.7972641048379,21.2400429812672,26.2167067042058));
#53107=CARTESIAN_POINT('Ctrl Pts',(-25.8288304974965,21.2708108719084,26.2139881026536));
#53108=CARTESIAN_POINT('Ctrl Pts',(-25.8574180644152,21.2997504965842,26.2115222281589));
#53109=CARTESIAN_POINT('Ctrl Pts',(-25.9492087658228,21.3962596959981,26.2035601964081));
#53110=CARTESIAN_POINT('Ctrl Pts',(-26.0100553949186,21.4660143221509,26.198210151161));
#53111=CARTESIAN_POINT('Ctrl Pts',(-26.1111589222809,21.5925255183622,26.1889948487992));
#53112=CARTESIAN_POINT('Ctrl Pts',(-26.1527349483438,21.6481425484671,26.1850950506388));
#53113=CARTESIAN_POINT('Ctrl Pts',(-26.254611860594,21.7940256160188,26.1751346025429));
#53114=CARTESIAN_POINT('Ctrl Pts',(-26.3122073117956,21.8860717009852,26.1690984212877));
#53115=CARTESIAN_POINT('Ctrl Pts',(-26.4604574783865,22.1519646583804,26.1519436513561));
#53116=CARTESIAN_POINT('Ctrl Pts',(-26.540048547062,22.3313989015759,26.1406583979027));
#53117=CARTESIAN_POINT('Ctrl Pts',(-26.606945467091,22.5290234585465,26.1279815015744));
#53118=CARTESIAN_POINT('Ctrl Pts',(-26.6109665920806,22.5411390820017,26.127203528246));
#53119=CARTESIAN_POINT('Ctrl Pts',(-26.6163525516445,22.5576953260091,26.126139219398));
#53120=CARTESIAN_POINT('Ctrl Pts',(-26.6177799612247,22.5621155940141,26.1258549494743));
#53121=CARTESIAN_POINT('Ctrl Pts',(-26.6201901744655,22.5696348683179,26.1253711788046));
#53122=CARTESIAN_POINT('Ctrl Pts',(-26.6211778572934,22.5727323136388,26.1251718390381));
#53123=CARTESIAN_POINT('Ctrl Pts',(-26.6230768532445,22.5787189864511,26.124786445186));
#53124=CARTESIAN_POINT('Ctrl Pts',(-26.623988782861,22.5816080154713,26.1246004116717));
#53125=CARTESIAN_POINT('Ctrl Pts',(-26.6261395423733,22.5884553270966,26.1241593682908));
#53126=CARTESIAN_POINT('Ctrl Pts',(-26.627374805036,22.5924147166732,26.1239042414472));
#53127=CARTESIAN_POINT('Ctrl Pts',(-26.6309838726525,22.6040619036301,26.123153450393));
#53128=CARTESIAN_POINT('Ctrl Pts',(-26.6333365218117,22.6117561769875,26.1226570924428));
#53129=CARTESIAN_POINT('Ctrl Pts',(-26.6385768769098,22.6291269837464,26.1215356200054));
#53130=CARTESIAN_POINT('Ctrl Pts',(-26.6414479545181,22.6388084080591,26.120909965218));
#53131=CARTESIAN_POINT('Ctrl Pts',(-26.6504721290202,22.6697715371631,26.1189069518365));
#53132=CARTESIAN_POINT('Ctrl Pts',(-26.6564512067717,22.6911029028437,26.1175239382748));
#53133=CARTESIAN_POINT('Ctrl Pts',(-26.736013732696,22.9866476313332,26.0983168638294));
#53134=CARTESIAN_POINT('Ctrl Pts',(-26.7732476569941,23.2692853830247,26.0792408559392));
#53135=CARTESIAN_POINT('Ctrl Pts',(-26.7730013173331,23.5530502384158,26.0600382396916));
#53136=CARTESIAN_POINT('Ctrl Pts',(-22.0750360153461,26.4155367745563,25.653793035611));
#53137=CARTESIAN_POINT('Ctrl Pts',(-22.1636145467195,26.4611422019415,25.6599527331432));
#53138=CARTESIAN_POINT('Ctrl Pts',(-22.2544190940411,26.5026924933022,25.6661124306754));
#53139=CARTESIAN_POINT('Ctrl Pts',(-22.3470417866287,26.5399684823254,25.6722721282076));
#53140=CARTESIAN_POINT('Ctrl Pts',(-22.4417132505225,26.5780689990598,25.6785680754125));
#53141=CARTESIAN_POINT('Ctrl Pts',(-22.5382838620969,26.6117036240226,25.6848640226175));
#53142=CARTESIAN_POINT('Ctrl Pts',(-22.6362924949834,26.6406885225854,25.6911599698225));
#53143=CARTESIAN_POINT('Ctrl Pts',(-22.7320460985457,26.6690065227915,25.6973110568743));
#53144=CARTESIAN_POINT('Ctrl Pts',(-22.8291718214375,26.6928863357309,25.7034621439261));
#53145=CARTESIAN_POINT('Ctrl Pts',(-22.9272218171399,26.7122060878398,25.709613230978));
#53146=CARTESIAN_POINT('Ctrl Pts',(-23.025250537181,26.7315216477965,25.7157629833184));
#53147=CARTESIAN_POINT('Ctrl Pts',(-23.1242027053701,26.7462790294842,25.7219127356589));
#53148=CARTESIAN_POINT('Ctrl Pts',(-23.2236194282402,26.7564072968651,25.7280624879993));
#53149=CARTESIAN_POINT('Ctrl Pts',(-23.3230411756617,26.7665360761317,25.7342125511501));
#53150=CARTESIAN_POINT('Ctrl Pts',(-23.4229270921102,26.7720352328171,25.7403626143009));
#53151=CARTESIAN_POINT('Ctrl Pts',(-23.5228133023489,26.7728857176452,25.7465126774517));
#53152=CARTESIAN_POINT('Ctrl Pts',(-23.6268430232608,26.7737714825481,25.7529178594247));
#53153=CARTESIAN_POINT('Ctrl Pts',(-23.7308725498221,26.7696145252937,25.7593230413976));
#53154=CARTESIAN_POINT('Ctrl Pts',(-23.8343797818175,26.7604533460106,25.7657282233706));
#53155=CARTESIAN_POINT('Ctrl Pts',(-23.9339131021665,26.7516438882096,25.7718874937609));
#53156=CARTESIAN_POINT('Ctrl Pts',(-24.032963063677,26.7382075168608,25.7780467641512));
#53157=CARTESIAN_POINT('Ctrl Pts',(-24.1310738740573,26.7202311011416,25.7842060345414));
#53158=CARTESIAN_POINT('Ctrl Pts',(-24.2292546594097,26.7022418642135,25.7903696978704));
#53159=CARTESIAN_POINT('Ctrl Pts',(-24.3264945383187,26.6797062357736,25.7965333611993));
#53160=CARTESIAN_POINT('Ctrl Pts',(-24.4223514623728,26.652761358049,25.8026970245283));
#53161=CARTESIAN_POINT('Ctrl Pts',(-24.5183509782933,26.6257763984999,25.8088698566081));
#53162=CARTESIAN_POINT('Ctrl Pts',(-24.6129630252629,26.5943692422234,25.815042688688));
#53163=CARTESIAN_POINT('Ctrl Pts',(-24.7057644460702,26.5587255294515,25.8212155207679));
#53164=CARTESIAN_POINT('Ctrl Pts',(-24.7165855111701,26.5545693114438,25.8219353008877));
#53165=CARTESIAN_POINT('Ctrl Pts',(-24.7273819850634,26.5503555421446,25.8226550810075));
#53166=CARTESIAN_POINT('Ctrl Pts',(-24.7381532190843,26.5460845562573,25.8233748611273));
#53167=CARTESIAN_POINT('Ctrl Pts',(-24.8305162082613,26.5094609881022,25.8295469527638));
#53168=CARTESIAN_POINT('Ctrl Pts',(-24.9213465968592,26.468497520667,25.8357190444003));
#53169=CARTESIAN_POINT('Ctrl Pts',(-25.0102075054303,26.4233430344739,25.8418911360368));
#53170=CARTESIAN_POINT('Ctrl Pts',(-25.0989480162784,26.3782497281339,25.8480548651009));
#53171=CARTESIAN_POINT('Ctrl Pts',(-25.1857239670718,26.3289768845462,25.854218594165));
#53172=CARTESIAN_POINT('Ctrl Pts',(-25.2701170629948,26.2757219511656,25.8603823232291));
#53173=CARTESIAN_POINT('Ctrl Pts',(-25.3544207523686,26.2225234363792,25.8665395224019));
#53174=CARTESIAN_POINT('Ctrl Pts',(-25.4363462402853,26.1653514494029,25.8726967215746));
#53175=CARTESIAN_POINT('Ctrl Pts',(-25.5154993923776,26.1044495364442,25.8788539207474));
#53176=CARTESIAN_POINT('Ctrl Pts',(-25.594594688316,26.0435921390905,25.885006619381));
#53177=CARTESIAN_POINT('Ctrl Pts',(-25.6709213340261,25.9790105002969,25.8911593180145));
#53178=CARTESIAN_POINT('Ctrl Pts',(-25.7441145614843,25.9109911781236,25.8973120166481));
#53179=CARTESIAN_POINT('Ctrl Pts',(-25.8172800339653,25.8429976489752,25.9034623821695));
#53180=CARTESIAN_POINT('Ctrl Pts',(-25.8873141312736,25.771569322023,25.909612747691));
#53181=CARTESIAN_POINT('Ctrl Pts',(-25.9538862370753,25.6970321134995,25.9157631132124));
#53182=CARTESIAN_POINT('Ctrl Pts',(-26.020450908631,25.6225032287015,25.9219127919096));
#53183=CARTESIAN_POINT('Ctrl Pts',(-26.0835540679393,25.5448664765553,25.9280624706069));
#53184=CARTESIAN_POINT('Ctrl Pts',(-26.1429036530184,25.4644828536765,25.9342121493041));
#53185=CARTESIAN_POINT('Ctrl Pts',(-26.2022624880375,25.384086702594,25.9403627864606));
#53186=CARTESIAN_POINT('Ctrl Pts',(-26.257866328792,25.3009431799375,25.9465134236172));
#53187=CARTESIAN_POINT('Ctrl Pts',(-26.3094655212953,25.2154435839512,25.9526640607737));
#53188=CARTESIAN_POINT('Ctrl Pts',(-26.361119914063,25.1298525214112,25.9588212778161));
#53189=CARTESIAN_POINT('Ctrl Pts',(-26.4087608787012,25.0419007249948,25.9649784948585));
#53190=CARTESIAN_POINT('Ctrl Pts',(-26.4521840362903,24.952005400474,25.9711357119009));
#53191=CARTESIAN_POINT('Ctrl Pts',(-26.4956314194697,24.8620599237436,25.9772963640278));
#53192=CARTESIAN_POINT('Ctrl Pts',(-26.5348561388962,24.7701691591104,25.9834570161547));
#53193=CARTESIAN_POINT('Ctrl Pts',(-26.5697022492787,24.6767697155308,25.9896176682817));
#53194=CARTESIAN_POINT('Ctrl Pts',(-26.60460666956,24.5832139815631,25.9957886293641));
#53195=CARTESIAN_POINT('Ctrl Pts',(-26.6351177125498,24.4881449397316,26.0019595904466));
#53196=CARTESIAN_POINT('Ctrl Pts',(-26.6611294783929,24.3920138903929,26.0081305515291));
#53197=CARTESIAN_POINT('Ctrl Pts',(-26.6809847330347,24.3186353095189,26.0128409585201));
#53198=CARTESIAN_POINT('Ctrl Pts',(-26.6982194975119,24.2446382499281,26.0175513655111));
#53199=CARTESIAN_POINT('Ctrl Pts',(-26.7128069574075,24.1702259721747,26.0222617725022));
#53200=CARTESIAN_POINT('Ctrl Pts',(-26.7407090601528,24.027894199937,26.031271583722));
#53201=CARTESIAN_POINT('Ctrl Pts',(-26.7590096370179,23.8836232293146,26.0402813949418));
#53202=CARTESIAN_POINT('Ctrl Pts',(-26.7675014364373,23.7384732729247,26.0492912061617));
#53203=CARTESIAN_POINT('Ctrl Pts',(-26.7711087967177,23.6768128212911,26.0531186205321));
#53204=CARTESIAN_POINT('Ctrl Pts',(-26.7729465872607,23.614994050472,26.0569460349024));
#53205=CARTESIAN_POINT('Ctrl Pts',(-26.7730012737579,23.5530999914162,26.0607734492728));
#53206=CARTESIAN_POINT('',(-26.7730026521799,23.5484313703039,25.8164188470677));
#53207=CARTESIAN_POINT('Ctrl Pts',(-22.0750361607755,26.4155368494318,25.4084140214669));
#53208=CARTESIAN_POINT('Ctrl Pts',(-22.1782012019014,26.4686522616209,25.4162323515028));
#53209=CARTESIAN_POINT('Ctrl Pts',(-22.2842020110658,26.5161790568714,25.4239739883152));
#53210=CARTESIAN_POINT('Ctrl Pts',(-22.4005170944886,26.5609498395686,25.4320063618042));
#53211=CARTESIAN_POINT('Ctrl Pts',(-22.4084642392242,26.5639727167167,25.4325528924445));
#53212=CARTESIAN_POINT('Ctrl Pts',(-22.4470690419364,26.578482307905,25.4351964379665));
#53213=CARTESIAN_POINT('Ctrl Pts',(-22.4778899708359,26.5895333896195,25.4372723875315));
#53214=CARTESIAN_POINT('Ctrl Pts',(-22.5136306701617,26.6017370765861,25.4396356913983));
#53215=CARTESIAN_POINT('Ctrl Pts',(-22.5183897750248,26.6033496581765,25.439949486294));
#53216=CARTESIAN_POINT('Ctrl Pts',(-22.5254457836472,26.6057221428194,25.4404133847563));
#53217=CARTESIAN_POINT('Ctrl Pts',(-22.5277397735785,26.606490590965,25.4405639933222));
#53218=CARTESIAN_POINT('Ctrl Pts',(-22.5318145470433,26.6078504704126,25.4408311408059));
#53219=CARTESIAN_POINT('Ctrl Pts',(-22.5335949809529,26.6084429293028,25.4409477410013));
#53220=CARTESIAN_POINT('Ctrl Pts',(-22.537317802918,26.609678128708,25.441191280742));
#53221=CARTESIAN_POINT('Ctrl Pts',(-22.5392602806046,26.6103205728849,25.4413182023298));
#53222=CARTESIAN_POINT('Ctrl Pts',(-22.5443879424781,26.6120110516273,25.4416528475676));
#53223=CARTESIAN_POINT('Ctrl Pts',(-22.5475741635347,26.6130559691499,25.4418603856741));
#53224=CARTESIAN_POINT('Ctrl Pts',(-22.5617158009588,26.6176692703367,25.4427797526757));
#53225=CARTESIAN_POINT('Ctrl Pts',(-22.5726888549657,26.6211839187399,25.4434884318982));
#53226=CARTESIAN_POINT('Ctrl Pts',(-22.6016788638739,26.6302982312593,25.4453489329733));
#53227=CARTESIAN_POINT('Ctrl Pts',(-22.6197268368355,26.6357987530522,25.4464952512587));
#53228=CARTESIAN_POINT('Ctrl Pts',(-22.7011298730619,26.659828924516,25.4516162941497));
#53229=CARTESIAN_POINT('Ctrl Pts',(-22.7650010829774,26.6765692228039,25.4555007957022));
#53230=CARTESIAN_POINT('Ctrl Pts',(-22.9192179937474,26.7119633715666,25.4646601615215));
#53231=CARTESIAN_POINT('Ctrl Pts',(-23.0099389049544,26.7287243312666,25.4698714113415));
#53232=CARTESIAN_POINT('Ctrl Pts',(-23.4117502720847,26.7852561583849,25.4926386317475));
#53233=CARTESIAN_POINT('Ctrl Pts',(-23.7269098273122,26.7833939247232,25.5098773080211));
#53234=CARTESIAN_POINT('Ctrl Pts',(-24.0553628773759,26.7332279385035,25.5299902788652));
#53235=CARTESIAN_POINT('Ctrl Pts',(-24.0738666893163,26.7302363512263,25.5311299332376));
#53236=CARTESIAN_POINT('Ctrl Pts',(-24.098305665065,26.7260661146142,25.5326441616666));
#53237=CARTESIAN_POINT('Ctrl Pts',(-24.1042653687441,26.7250318824605,25.5330141337573));
#53238=CARTESIAN_POINT('Ctrl Pts',(-24.1135119849006,26.7234004184462,25.5335892704376));
#53239=CARTESIAN_POINT('Ctrl Pts',(-24.1168009618476,26.7228148398264,25.5337940633004));
#53240=CARTESIAN_POINT('Ctrl Pts',(-24.1233833800959,26.7216323254471,25.534204368993));
#53241=CARTESIAN_POINT('Ctrl Pts',(-24.1266768138055,26.7210353707535,25.5344098821989));
#53242=CARTESIAN_POINT('Ctrl Pts',(-24.1340264653712,26.7196913728574,25.5348690046711));
#53243=CARTESIAN_POINT('Ctrl Pts',(-24.1380821858119,26.7189416724907,25.5351226984782));
#53244=CARTESIAN_POINT('Ctrl Pts',(-24.149935983983,26.7167269553963,25.535865174975));
#53245=CARTESIAN_POINT('Ctrl Pts',(-24.1577300622579,26.7152409308774,25.5363546282118));
#53246=CARTESIAN_POINT('Ctrl Pts',(-24.2146960346144,26.7041615828578,25.5399413233347));
#53247=CARTESIAN_POINT('Ctrl Pts',(-24.2636414370363,26.6934520615622,25.5430741426074));
#53248=CARTESIAN_POINT('Ctrl Pts',(-24.4223347989986,26.6548316156612,25.5534068045175));
#53249=CARTESIAN_POINT('Ctrl Pts',(-24.5308550985955,26.6222799612034,25.560752369686));
#53250=CARTESIAN_POINT('Ctrl Pts',(-24.7567814515174,26.5413192307102,25.576624419732));
#53251=CARTESIAN_POINT('Ctrl Pts',(-24.8734996539564,26.491545677167,25.5851744107897));
#53252=CARTESIAN_POINT('Ctrl Pts',(-25.0424115468596,26.4074214870876,25.5979458933017));
#53253=CARTESIAN_POINT('Ctrl Pts',(-25.097040522891,26.378219998058,25.6021408588672));
#53254=CARTESIAN_POINT('Ctrl Pts',(-25.2251595773539,26.3049112614838,25.6120944940392));
#53255=CARTESIAN_POINT('Ctrl Pts',(-25.2978025412706,26.2594090276105,25.6178326945842));
#53256=CARTESIAN_POINT('Ctrl Pts',(-25.3770751519917,26.2052371480579,25.6241399427837));
#53257=CARTESIAN_POINT('Ctrl Pts',(-25.3855731016868,26.199369858123,25.6248166637968));
#53258=CARTESIAN_POINT('Ctrl Pts',(-25.4002707129897,26.1891174300168,25.6259879225723));
#53259=CARTESIAN_POINT('Ctrl Pts',(-25.4064833100331,26.1847510650331,25.6264832687521));
#53260=CARTESIAN_POINT('Ctrl Pts',(-25.4134175068567,26.1798408366279,25.6270363940962));
#53261=CARTESIAN_POINT('Ctrl Pts',(-25.4141543272033,26.179318615843,25.6270951716979));
#53262=CARTESIAN_POINT('Ctrl Pts',(-25.4173055060694,26.177083229976,25.6273465603261));
#53263=CARTESIAN_POINT('Ctrl Pts',(-25.4197177300441,26.1753670432597,25.6275390305066));
#53264=CARTESIAN_POINT('Ctrl Pts',(-25.426080558524,26.1708269644805,25.6280467963155));
#53265=CARTESIAN_POINT('Ctrl Pts',(-25.4300271657867,26.167997452343,25.6283618234762));
#53266=CARTESIAN_POINT('Ctrl Pts',(-25.4371436187509,26.162870933195,25.6289299991719));
#53267=CARTESIAN_POINT('Ctrl Pts',(-25.4403156960136,26.1605770558581,25.6291833017423));
#53268=CARTESIAN_POINT('Ctrl Pts',(-25.4800553960131,26.1317290046662,25.6323571544011));
#53269=CARTESIAN_POINT('Ctrl Pts',(-25.5160671063167,26.1044125608642,25.63523846938));
#53270=CARTESIAN_POINT('Ctrl Pts',(-25.5557593159857,26.0729672806974,25.6384091669173));
#53271=CARTESIAN_POINT('Ctrl Pts',(-25.5600155961446,26.0695777573212,25.6387490999583));
#53272=CARTESIAN_POINT('Ctrl Pts',(-25.56604804123,26.0647487541318,25.6392307673663));
#53273=CARTESIAN_POINT('Ctrl Pts',(-25.5678312597824,26.063318162545,25.6393731353698));
#53274=CARTESIAN_POINT('Ctrl Pts',(-25.571097159376,26.0606923696666,25.6396338470576));
#53275=CARTESIAN_POINT('Ctrl Pts',(-25.5725803054489,26.0594977498564,25.6397522328894));
#53276=CARTESIAN_POINT('Ctrl Pts',(-25.575424061759,26.057203049299,25.6399792003166));
#53277=CARTESIAN_POINT('Ctrl Pts',(-25.5767848340962,26.0561031759387,25.6400877968286));
#53278=CARTESIAN_POINT('Ctrl Pts',(-25.5796492185803,26.0537841166751,25.6403163693369));
#53279=CARTESIAN_POINT('Ctrl Pts',(-25.5811526301685,26.052564682447,25.6404363272161));
#53280=CARTESIAN_POINT('Ctrl Pts',(-25.5865619176092,26.0481690617834,25.6408678988277));
#53281=CARTESIAN_POINT('Ctrl Pts',(-25.5904614752363,26.0449850572294,25.6411789478602));
#53282=CARTESIAN_POINT('Ctrl Pts',(-25.6341933784183,26.0091066639358,25.6446666381402));
#53283=CARTESIAN_POINT('Ctrl Pts',(-25.6732462992263,25.9754682549462,25.6477756331427));
#53284=CARTESIAN_POINT('Ctrl Pts',(-25.7656509124129,25.8919315624595,25.655165822624));
#53285=CARTESIAN_POINT('Ctrl Pts',(-25.8181469271391,25.8411272723573,25.6593931983228));
#53286=CARTESIAN_POINT('Ctrl Pts',(-26.0792168655783,25.5706920896179,25.6808496932107));
#53287=CARTESIAN_POINT('Ctrl Pts',(-26.2577930040983,25.3242517755272,25.6971805666352));
#53288=CARTESIAN_POINT('Ctrl Pts',(-26.4088533530779,25.0385174521646,25.7161160433643));
#53289=CARTESIAN_POINT('Ctrl Pts',(-26.4181875845009,25.020449673942,25.7173125935699));
#53290=CARTESIAN_POINT('Ctrl Pts',(-26.4294071580061,24.9982190525818,25.7187844820835));
#53291=CARTESIAN_POINT('Ctrl Pts',(-26.4314555944326,24.9941387179275,25.7190546263805));
#53292=CARTESIAN_POINT('Ctrl Pts',(-26.4352951885162,24.9864498234203,25.7195636632746));
#53293=CARTESIAN_POINT('Ctrl Pts',(-26.437088265474,24.9828422281563,25.7198024940292));
#53294=CARTESIAN_POINT('Ctrl Pts',(-26.4407208614247,24.9754990842243,25.7202886191982));
#53295=CARTESIAN_POINT('Ctrl Pts',(-26.4425599141645,24.9717633145413,25.7205359280052));
#53296=CARTESIAN_POINT('Ctrl Pts',(-26.4676050521694,24.9206379274791,25.723920442057));
#53297=CARTESIAN_POINT('Ctrl Pts',(-26.4896499872633,24.8726911743882,25.7270947500384));
#53298=CARTESIAN_POINT('Ctrl Pts',(-26.5139557150827,24.816213475613,25.730841764078));
#53299=CARTESIAN_POINT('Ctrl Pts',(-26.5173717918601,24.8081861405744,25.731374516148));
#53300=CARTESIAN_POINT('Ctrl Pts',(-26.5224176604426,24.7961940969756,25.7321706953239));
#53301=CARTESIAN_POINT('Ctrl Pts',(-26.5240722236245,24.7922398006507,25.7324332786025));
#53302=CARTESIAN_POINT('Ctrl Pts',(-26.5270106111623,24.7851777137988,25.732902324462));
#53303=CARTESIAN_POINT('Ctrl Pts',(-26.5282974724468,24.782071187096,25.7331086834715));
#53304=CARTESIAN_POINT('Ctrl Pts',(-26.5310017230855,24.7755140288462,25.7335443282901));
#53305=CARTESIAN_POINT('Ctrl Pts',(-26.5324179868285,24.7720629410458,25.7337736519299));
#53306=CARTESIAN_POINT('Ctrl Pts',(-26.5361462471653,24.7629329831652,25.7343804447327));
#53307=CARTESIAN_POINT('Ctrl Pts',(-26.5384480263752,24.7572499808242,25.7347582593922));
#53308=CARTESIAN_POINT('Ctrl Pts',(-26.5488198081606,24.7314309418125,25.7364752888727));
#53309=CARTESIAN_POINT('Ctrl Pts',(-26.5567024411274,24.7112206850176,25.7378208149143));
#53310=CARTESIAN_POINT('Ctrl Pts',(-26.6131846603531,24.5619723526261,25.7477700388037));
#53311=CARTESIAN_POINT('Ctrl Pts',(-26.6536557769766,24.4300306002522,25.7566450565172));
#53312=CARTESIAN_POINT('Ctrl Pts',(-26.7438013880824,24.0509953044662,25.7823544411515));
#53313=CARTESIAN_POINT('Ctrl Pts',(-26.7731438782448,23.8001313092259,25.7996825319716));
#53314=CARTESIAN_POINT('Ctrl Pts',(-26.7730020198273,23.548436151331,25.8164196296698));
#53315=CARTESIAN_POINT('Ctrl Pts',(-26.7730020171705,23.5484314435376,25.8164199427262));
#53316=CARTESIAN_POINT('Ctrl Pts',(-26.7729508853726,23.4579443493913,25.8224371045826));
#53317=CARTESIAN_POINT('Ctrl Pts',(-26.7690887550542,23.3674885436758,25.8283579034823));
#53318=CARTESIAN_POINT('Ctrl Pts',(-26.7601466049889,23.2622858317644,25.8350467304567));
#53319=CARTESIAN_POINT('Ctrl Pts',(-26.7587645555835,23.2472749821746,25.8359963976571));
#53320=CARTESIAN_POINT('Ctrl Pts',(-26.7568975818284,23.2284453095156,25.8371812592684));
#53321=CARTESIAN_POINT('Ctrl Pts',(-26.7565111022516,23.2246172374036,25.8374218089649));
#53322=CARTESIAN_POINT('Ctrl Pts',(-26.7558695388139,23.2183744487913,25.8378135425975));
#53323=CARTESIAN_POINT('Ctrl Pts',(-26.7556185811685,23.215959326234,25.8379649560027));
#53324=CARTESIAN_POINT('Ctrl Pts',(-26.7551715203555,23.2117037697322,25.8382315126332));
#53325=CARTESIAN_POINT('Ctrl Pts',(-26.7549765611708,23.209863220692,25.8383467203063));
#53326=CARTESIAN_POINT('Ctrl Pts',(-26.7545902212932,23.2062456598311,25.8385730011819));
#53327=CARTESIAN_POINT('Ctrl Pts',(-26.7543989475674,23.2044686359091,25.8386840805099));
#53328=CARTESIAN_POINT('Ctrl Pts',(-26.7540146535614,23.2009260606441,25.8389053720425));
#53329=CARTESIAN_POINT('Ctrl Pts',(-26.753821652477,23.1991605134247,25.8390155851057));
#53330=CARTESIAN_POINT('Ctrl Pts',(-26.7533575324538,23.1949470541703,25.8392784323874));
#53331=CARTESIAN_POINT('Ctrl Pts',(-26.7530850662469,23.1924992871875,25.8394309898803));
#53332=CARTESIAN_POINT('Ctrl Pts',(-26.7522531170804,23.1851023976257,25.8398915825659));
#53333=CARTESIAN_POINT('Ctrl Pts',(-26.7516849635077,23.1801542278042,25.8401991293191));
#53334=CARTESIAN_POINT('Ctrl Pts',(-26.7457771444037,23.1297334770029,25.8433273527712));
#53335=CARTESIAN_POINT('Ctrl Pts',(-26.7394801605924,23.0843754169231,25.8460949625909));
#53336=CARTESIAN_POINT('Ctrl Pts',(-26.7299435750956,23.0250019500297,25.8496746154563));
#53337=CARTESIAN_POINT('Ctrl Pts',(-26.7275742756882,23.0108548549804,25.8505243159767));
#53338=CARTESIAN_POINT('Ctrl Pts',(-26.7186564954646,22.9597054103027,25.8535862476331));
#53339=CARTESIAN_POINT('Ctrl Pts',(-26.7115552407843,22.9228013674714,25.855776071186));
#53340=CARTESIAN_POINT('Ctrl Pts',(-26.7010859111894,22.8730957865562,25.858709353206));
#53341=CARTESIAN_POINT('Ctrl Pts',(-26.6982823340377,22.8601796272125,25.8594700902017));
#53342=CARTESIAN_POINT('Ctrl Pts',(-26.634697175194,22.5756949260541,25.8761998852543));
#53343=CARTESIAN_POINT('Ctrl Pts',(-26.5390753079627,22.3131125466077,25.8912303861599));
#53344=CARTESIAN_POINT('Ctrl Pts',(-26.3729198947162,21.9928609820453,25.9120516557774));
#53345=CARTESIAN_POINT('Ctrl Pts',(-26.3321443967014,21.921143722296,25.9168842439819));
#53346=CARTESIAN_POINT('Ctrl Pts',(-26.2661969957937,21.8148622900479,25.9243613402459));
#53347=CARTESIAN_POINT('Ctrl Pts',(-26.2430131545674,21.7791021750985,25.9269337495212));
#53348=CARTESIAN_POINT('Ctrl Pts',(-26.2148670523715,21.7375184637387,25.9299965108269));
#53349=CARTESIAN_POINT('Ctrl Pts',(-26.2105839889066,21.7312385457294,25.9304609971542));
#53350=CARTESIAN_POINT('Ctrl Pts',(-26.2039827469513,21.7216328496996,25.9311744941909));
#53351=CARTESIAN_POINT('Ctrl Pts',(-26.2016804238545,21.7182961650793,25.9314229004665));
#53352=CARTESIAN_POINT('Ctrl Pts',(-26.1976525415448,21.7124821801752,25.9318567204163));
#53353=CARTESIAN_POINT('Ctrl Pts',(-26.1959297819071,21.710002938653,25.9320420269041));
#53354=CARTESIAN_POINT('Ctrl Pts',(-26.1920452790639,21.704429438859,25.9324593170946));
#53355=CARTESIAN_POINT('Ctrl Pts',(-26.1898815810993,21.7013365543057,25.932691375537));
#53356=CARTESIAN_POINT('Ctrl Pts',(-26.1840754730514,21.6930680145503,25.9333130876674));
#53357=CARTESIAN_POINT('Ctrl Pts',(-26.1804232559083,21.6878992951381,25.9337031179205));
#53358=CARTESIAN_POINT('Ctrl Pts',(-26.1645753422939,21.6656104867645,25.9353910931808));
#53359=CARTESIAN_POINT('Ctrl Pts',(-26.1522277577916,21.6485994916803,25.9366948948896));
#53360=CARTESIAN_POINT('Ctrl Pts',(-25.9284107165336,21.3465128610276,25.9601319614637));
#53361=CARTESIAN_POINT('Ctrl Pts',(-25.6714746131869,21.0982360920666,25.9843574315045));
#53362=CARTESIAN_POINT('Ctrl Pts',(-25.3215930923605,20.8570389379362,26.0129041989637));
#53363=CARTESIAN_POINT('Ctrl Pts',(-25.262498594258,20.8190877059489,26.0175830382128));
#53364=CARTESIAN_POINT('Ctrl Pts',(-25.1598770501091,20.757824004178,26.0254161594825));
#53365=CARTESIAN_POINT('Ctrl Pts',(-25.116968479097,20.7335257255886,26.0286083576628));
#53366=CARTESIAN_POINT('Ctrl Pts',(-25.0527088621478,20.6990597879695,26.0332495058558));
#53367=CARTESIAN_POINT('Ctrl Pts',(-25.0317781726435,20.6881279813832,26.0347398539775));
#53368=CARTESIAN_POINT('Ctrl Pts',(-25.006966932198,20.6755145394527,26.0364797891443));
#53369=CARTESIAN_POINT('Ctrl Pts',(-25.0032015948466,20.6736096291008,26.0367431205578));
#53370=CARTESIAN_POINT('Ctrl Pts',(-24.997781423168,20.6708808836015,26.0371211377086));
#53371=CARTESIAN_POINT('Ctrl Pts',(-24.9961296250947,20.6700510786162,26.0372361990192));
#53372=CARTESIAN_POINT('Ctrl Pts',(-24.9928776025667,20.6684208799986,26.0374624534011));
#53373=CARTESIAN_POINT('Ctrl Pts',(-24.9912774225979,20.667620396356,26.0375736521762));
#53374=CARTESIAN_POINT('Ctrl Pts',(-24.9880849262335,20.6660266854137,26.0377952406598));
#53375=CARTESIAN_POINT('Ctrl Pts',(-24.986492623176,20.6652334456572,26.0379056311315));
#53376=CARTESIAN_POINT('Ctrl Pts',(-24.9826845529548,20.6633403081693,26.0381693267425));
#53377=CARTESIAN_POINT('Ctrl Pts',(-24.9804681705585,20.6622416403862,26.0383225540196));
#53378=CARTESIAN_POINT('Ctrl Pts',(-24.9725232307422,20.65831469756,26.0388709336001));
#53379=CARTESIAN_POINT('Ctrl Pts',(-24.966787481921,20.6555008818441,26.0392651816654));
#53380=CARTESIAN_POINT('Ctrl Pts',(-24.8815195804946,20.6139846913807,26.0451022255994));
#53381=CARTESIAN_POINT('Ctrl Pts',(-24.8004268548213,20.5785512889499,26.0503459803637));
#53382=CARTESIAN_POINT('Ctrl Pts',(-24.5866808818096,20.4954569826156,26.0636413162355));
#53383=CARTESIAN_POINT('Ctrl Pts',(-24.4521771527532,20.4530769175625,26.0715059635698));
#53384=CARTESIAN_POINT('Ctrl Pts',(-24.2990708004479,20.4156602589407,26.080312777012));
#53385=CARTESIAN_POINT('Ctrl Pts',(-24.2827866248665,20.4118148123829,26.0812475719305));
#53386=CARTESIAN_POINT('Ctrl Pts',(-24.2476428875576,20.4038041753138,26.0832620936102));
#53387=CARTESIAN_POINT('Ctrl Pts',(-24.2287743622989,20.3996813628218,26.0843418869993));
#53388=CARTESIAN_POINT('Ctrl Pts',(-24.1877018276741,20.3910930120451,26.0866901734016));
#53389=CARTESIAN_POINT('Ctrl Pts',(-24.1654855533632,20.3866914377482,26.087958993486));
#53390=CARTESIAN_POINT('Ctrl Pts',(-24.1164953718931,20.3775208840379,26.0907565717696));
#53391=CARTESIAN_POINT('Ctrl Pts',(-24.0897038804668,20.372855911909,26.0922862662849));
#53392=CARTESIAN_POINT('Ctrl Pts',(-24.0292965634924,20.3631237453181,26.0957392088235));
#53393=CARTESIAN_POINT('Ctrl Pts',(-23.9956534046897,20.3582482898633,26.0976650064516));
#53394=CARTESIAN_POINT('Ctrl Pts',(-23.8500453583177,20.3394940669868,26.106026815534));
#53395=CARTESIAN_POINT('Ctrl Pts',(-23.7374810321793,20.3309688461738,26.1125632030665));
#53396=CARTESIAN_POINT('Ctrl Pts',(-23.5747295719455,20.3272077474001,26.1222593671421));
#53397=CARTESIAN_POINT('Ctrl Pts',(-23.524732648307,20.3272159016937,26.1252707345463));
#53398=CARTESIAN_POINT('Ctrl Pts',(-23.4668301252195,20.3285726666372,26.1288025168985));
#53399=CARTESIAN_POINT('Ctrl Pts',(-23.4589028552326,20.3287876963043,26.1292870008526));
#53400=CARTESIAN_POINT('Ctrl Pts',(-23.446854931912,20.3291590058179,26.1300248052801));
#53401=CARTESIAN_POINT('Ctrl Pts',(-23.4427336116098,20.329293940272,26.1302774550432));
#53402=CARTESIAN_POINT('Ctrl Pts',(-23.4352675432404,20.3295527292253,26.1307356301612));
#53403=CARTESIAN_POINT('Ctrl Pts',(-23.4319227024627,20.3296738854614,26.1309410704571));
#53404=CARTESIAN_POINT('Ctrl Pts',(-23.4252392494024,20.3299263983091,26.1313519210974));
#53405=CARTESIAN_POINT('Ctrl Pts',(-23.4219006404829,20.3300577366543,26.1315573306216));
#53406=CARTESIAN_POINT('Ctrl Pts',(-23.4125160651701,20.33044153634,26.1321352187284));
#53407=CARTESIAN_POINT('Ctrl Pts',(-23.4064706203145,20.3307058336053,26.1325080688415));
#53408=CARTESIAN_POINT('Ctrl Pts',(-23.3816833132228,20.3318594497573,26.1340392228559));
#53409=CARTESIAN_POINT('Ctrl Pts',(-23.3629489410805,20.3328953938795,26.1352021260462));
#53410=CARTESIAN_POINT('Ctrl Pts',(-23.0328407098786,20.3540421758558,26.1557955897981));
#53411=CARTESIAN_POINT('Ctrl Pts',(-22.7260704502414,20.419101869334,26.1767891579853));
#53412=CARTESIAN_POINT('Ctrl Pts',(-22.3291076746122,20.5657403549522,26.2054076519512));
#53413=CARTESIAN_POINT('Ctrl Pts',(-22.2267549729426,20.6096973362167,26.212902006021));
#53414=CARTESIAN_POINT('Ctrl Pts',(-22.080044480779,20.6819201472966,26.2236416928645));
#53415=CARTESIAN_POINT('Ctrl Pts',(-22.033775885001,20.7061108957067,26.2270277861206));
#53416=CARTESIAN_POINT('Ctrl Pts',(-21.973682145234,20.7394135871053,26.2314051842126));
#53417=CARTESIAN_POINT('Ctrl Pts',(-21.9593128938971,20.7475215686462,26.2324502988225));
#53418=CARTESIAN_POINT('Ctrl Pts',(-21.9389925914881,20.7591941188688,26.2339253063251));
#53419=CARTESIAN_POINT('Ctrl Pts',(-21.9329900867101,20.7626679419748,26.2343606475492));
#53420=CARTESIAN_POINT('Ctrl Pts',(-21.9224717266498,20.768800631288,26.235122797681));
#53421=CARTESIAN_POINT('Ctrl Pts',(-21.9179510820558,20.7714511710396,26.2354501276282));
#53422=CARTESIAN_POINT('Ctrl Pts',(-21.9113244313939,20.7753582529353,26.2359295853252));
#53423=CARTESIAN_POINT('Ctrl Pts',(-21.9092133918809,20.7766061739298,26.2360822709452));
#53424=CARTESIAN_POINT('Ctrl Pts',(-21.9055668368967,20.7787674208277,26.2363459193962));
#53425=CARTESIAN_POINT('Ctrl Pts',(-21.9040306551724,20.7796796148139,26.2364569566381));
#53426=CARTESIAN_POINT('Ctrl Pts',(-21.9009697398967,20.7815006493575,26.2366781432636));
#53427=CARTESIAN_POINT('Ctrl Pts',(-21.8994450017755,20.7824094703078,26.23678829354));
#53428=CARTESIAN_POINT('Ctrl Pts',(-21.8958097904295,20.7845803122976,26.2370508397822));
#53429=CARTESIAN_POINT('Ctrl Pts',(-21.8937000054565,20.7858434922836,26.237203159424));
#53430=CARTESIAN_POINT('Ctrl Pts',(-21.887334559195,20.7896645449613,26.2376625625859));
#53431=CARTESIAN_POINT('Ctrl Pts',(-21.8830833360512,20.7922298541891,26.237969161151));
#53432=CARTESIAN_POINT('Ctrl Pts',(-21.8401342756492,20.8182821312639,26.2410646191982));
#53433=CARTESIAN_POINT('Ctrl Pts',(-21.8019270363729,20.8425736007255,26.2438016120632));
#53434=CARTESIAN_POINT('Ctrl Pts',(-21.7587193739858,20.871340341008,26.2468926952176));
#53435=CARTESIAN_POINT('Ctrl Pts',(-21.7532081049598,20.875034239612,26.2472868939016));
#53436=CARTESIAN_POINT('Ctrl Pts',(-21.7429709576011,20.8819415428572,26.2480190468523));
#53437=CARTESIAN_POINT('Ctrl Pts',(-21.7382421554303,20.8851505414584,26.2483572197616));
#53438=CARTESIAN_POINT('Ctrl Pts',(-21.7287239888428,20.891646680387,26.2490378948187));
#53439=CARTESIAN_POINT('Ctrl Pts',(-21.7239349257831,20.8949342253009,26.2493803753845));
#53440=CARTESIAN_POINT('Ctrl Pts',(-21.7106782230547,20.9040873761319,26.2503284774512));
#53441=CARTESIAN_POINT('Ctrl Pts',(-21.7022297191454,20.9099806979159,26.2509327882723));
#53442=CARTESIAN_POINT('Ctrl Pts',(-21.471097318003,21.0728618928778,26.267471975173));
#53443=CARTESIAN_POINT('Ctrl Pts',(-21.2691691651441,21.2574291729343,26.2821763424851));
#53444=CARTESIAN_POINT('Ctrl Pts',(-21.0636437686147,21.4996589771405,26.3002437269313));
#53445=CARTESIAN_POINT('Ctrl Pts',(-21.0351537744921,21.5347041933496,26.3028292636445));
#53446=CARTESIAN_POINT('Ctrl Pts',(-20.9572621302943,21.6347418075215,26.3101520601756));
#53447=CARTESIAN_POINT('Ctrl Pts',(-20.909582384188,21.7010256262659,26.3149388155384));
#53448=CARTESIAN_POINT('Ctrl Pts',(-20.8415811627579,21.8035606909281,26.3222981495056));
#53449=CARTESIAN_POINT('Ctrl Pts',(-20.8193581632005,21.8385140365042,26.3247991245502));
#53450=CARTESIAN_POINT('Ctrl Pts',(-20.7938928180428,21.8803257169855,26.3277853293147));
#53451=CARTESIAN_POINT('Ctrl Pts',(-20.7899925993808,21.8867803972526,26.3282461699932));
#53452=CARTESIAN_POINT('Ctrl Pts',(-20.7840373339764,21.8967146963561,26.3289552283832));
#53453=CARTESIAN_POINT('Ctrl Pts',(-20.7819660978303,21.9001846201139,26.3292028534018));
#53454=CARTESIAN_POINT('Ctrl Pts',(-20.7783595289985,21.9062525769688,26.3296358164609));
#53455=CARTESIAN_POINT('Ctrl Pts',(-20.776821305579,21.908848893511,26.3298210487214));
#53456=CARTESIAN_POINT('Ctrl Pts',(-20.7736069030334,21.9142917962262,26.3302093262963));
#53457=CARTESIAN_POINT('Ctrl Pts',(-20.7719314502176,21.9171388053268,26.3304123977856));
#53458=CARTESIAN_POINT('Ctrl Pts',(-20.7672942192439,21.925046398501,26.3309763667922));
#53459=CARTESIAN_POINT('Ctrl Pts',(-20.7643418813443,21.9301124785677,26.3313376068516));
#53460=CARTESIAN_POINT('Ctrl Pts',(-20.7527043721091,21.9502077923815,26.3327702530183));
#53461=CARTESIAN_POINT('Ctrl Pts',(-20.7441269858956,21.9652988177824,26.3338455518609));
#53462=CARTESIAN_POINT('Ctrl Pts',(-20.604211203519,22.2161623937189,26.3517133179768));
#53463=CARTESIAN_POINT('Ctrl Pts',(-20.5029078199641,22.4673937076515,26.3696398798604));
#53464=CARTESIAN_POINT('Ctrl Pts',(-20.3947658789947,22.8773471990841,26.3983271450534));
#53465=CARTESIAN_POINT('Ctrl Pts',(-20.3661836330995,23.0290925691655,26.4087996564778));
#53466=CARTESIAN_POINT('Ctrl Pts',(-20.3425919101127,23.2343762220688,26.4223761162917));
#53467=CARTESIAN_POINT('Ctrl Pts',(-20.3378787413927,23.2865864023653,26.4257774236067));
#53468=CARTESIAN_POINT('Ctrl Pts',(-20.3333326568256,23.3557540542404,26.4301957996883));
#53469=CARTESIAN_POINT('Ctrl Pts',(-20.3323569729912,23.3726255610273,26.4312666528582));
#53470=CARTESIAN_POINT('Ctrl Pts',(-20.3311619197704,23.3965546928009,26.4327749678696));
#53471=CARTESIAN_POINT('Ctrl Pts',(-20.3308329789276,23.4036062262066,26.4332181532725));
#53472=CARTESIAN_POINT('Ctrl Pts',(-20.3303662246702,23.4143719041332,26.4338927419989));
#53473=CARTESIAN_POINT('Ctrl Pts',(-20.3302116648933,23.4180852453961,26.4341250555352));
#53474=CARTESIAN_POINT('Ctrl Pts',(-20.3299376401443,23.4249547379125,26.4345541320549));
#53475=CARTESIAN_POINT('Ctrl Pts',(-20.3298163908399,23.4281108076669,26.434750993828));
#53476=CARTESIAN_POINT('Ctrl Pts',(-20.3296259007067,23.4332667611471,26.4350721528332));
#53477=CARTESIAN_POINT('Ctrl Pts',(-20.329553882903,23.4352665305314,26.4351966066318));
#53478=CARTESIAN_POINT('Ctrl Pts',(-20.3294174855085,23.439154656967,26.435438365469));
#53479=CARTESIAN_POINT('Ctrl Pts',(-20.3293529042015,23.4410429985073,26.4355556813166));
#53480=CARTESIAN_POINT('Ctrl Pts',(-20.3292077262896,23.4454001331403,26.4358261480431));
#53481=CARTESIAN_POINT('Ctrl Pts',(-20.3291283071146,23.4478689693839,26.4359792321525));
#53482=CARTESIAN_POINT('Ctrl Pts',(-20.3289230664606,23.4544858319803,26.436389078038));
#53483=CARTESIAN_POINT('Ctrl Pts',(-20.3288024179608,23.4586340317031,26.4366455491805));
#53484=CARTESIAN_POINT('Ctrl Pts',(-20.3280166577791,23.4875739453529,26.4384316359929));
#53485=CARTESIAN_POINT('Ctrl Pts',(-20.3276297049508,23.5123732634944,26.4399458782074));
#53486=CARTESIAN_POINT('Ctrl Pts',(-20.3274949192065,23.545590006885,26.4419552038689));
#53487=CARTESIAN_POINT('Ctrl Pts',(-20.3274937302696,23.5540047335916,26.4424625993338));
#53488=CARTESIAN_POINT('Ctrl Pts',(-20.3287910921516,23.897644647954,26.4631207995232));
#53489=CARTESIAN_POINT('Ctrl Pts',(-20.3823499015367,24.230669251405,26.4808845516421));
#53490=CARTESIAN_POINT('Ctrl Pts',(-20.5306399230803,24.6853666129075,26.5082645827915));
#53491=CARTESIAN_POINT('Ctrl Pts',(-20.5839377275395,24.8181296907315,26.5166449296376));
#53492=CARTESIAN_POINT('Ctrl Pts',(-20.6504526389001,24.9564496240396,26.525985672453));
#53493=CARTESIAN_POINT('Ctrl Pts',(-20.6550884118073,24.9659694509557,26.5266317015572));
#53494=CARTESIAN_POINT('Ctrl Pts',(-20.6618230931939,24.9796280855771,26.52756320589));
#53495=CARTESIAN_POINT('Ctrl Pts',(-20.6638841920089,24.9837855458026,26.5278473572804));
#53496=CARTESIAN_POINT('Ctrl Pts',(-20.6674778999292,24.9909952742325,26.52834120121));
#53497=CARTESIAN_POINT('Ctrl Pts',(-20.6690063992213,24.9940495921184,26.5285507492604));
#53498=CARTESIAN_POINT('Ctrl Pts',(-20.671955476274,24.9999192407727,26.5289540998495));
#53499=CARTESIAN_POINT('Ctrl Pts',(-20.6733753372938,25.0027349291338,26.5291478770076));
#53500=CARTESIAN_POINT('Ctrl Pts',(-20.676731053913,25.0093653370977,26.5296048681879));
#53501=CARTESIAN_POINT('Ctrl Pts',(-20.6786703734999,25.0131782887401,26.5298682040771));
#53502=CARTESIAN_POINT('Ctrl Pts',(-20.6844233627734,25.0244338890179,26.5306471412632));
#53503=CARTESIAN_POINT('Ctrl Pts',(-20.6882583951468,25.031865524338,26.5311634963251));
#53504=CARTESIAN_POINT('Ctrl Pts',(-20.7222966830311,25.0972006008343,26.5357212872539));
#53505=CARTESIAN_POINT('Ctrl Pts',(-20.7542226796643,25.1541847834394,26.539823700541));
#53506=CARTESIAN_POINT('Ctrl Pts',(-20.7968742523831,25.2251651263367,26.5451032752371));
#53507=CARTESIAN_POINT('Ctrl Pts',(-20.8060147407314,25.2400995888116,26.5462238669561));
#53508=CARTESIAN_POINT('Ctrl Pts',(-20.827624559586,25.2747696948877,26.5488482074975));
#53509=CARTESIAN_POINT('Ctrl Pts',(-20.8401874214789,25.2944456333662,26.5503551129478));
#53510=CARTESIAN_POINT('Ctrl Pts',(-21.009939759627,25.5540495088953,26.5704712282139));
#53511=CARTESIAN_POINT('Ctrl Pts',(-21.1982566725404,25.7720672581973,26.5902098732285));
#53512=CARTESIAN_POINT('Ctrl Pts',(-21.500121990606,26.0395642895927,26.61714482083));
#53513=CARTESIAN_POINT('Ctrl Pts',(-21.5915157639048,26.1121005769147,26.6247910373325));
#53514=CARTESIAN_POINT('Ctrl Pts',(-21.6905218161546,26.182274898733,26.6324024396636));
#53515=CARTESIAN_POINT('Ctrl Pts',(-21.6943988807157,26.1850100730518,26.632699470715));
#53516=CARTESIAN_POINT('Ctrl Pts',(-21.7005741331281,26.1893461694144,26.6331709165183));
#53517=CARTESIAN_POINT('Ctrl Pts',(-21.7028683732334,26.1909526619607,26.6333457068405));
#53518=CARTESIAN_POINT('Ctrl Pts',(-21.707184314151,26.1939664299064,26.6336738393385));
#53519=CARTESIAN_POINT('Ctrl Pts',(-21.7092055374242,26.1953743805137,26.6338272276013));
#53520=CARTESIAN_POINT('Ctrl Pts',(-21.7127632412056,26.1978465646149,26.6340967202118));
#53521=CARTESIAN_POINT('Ctrl Pts',(-21.7142990355046,26.1989117803926,26.6342128924386));
#53522=CARTESIAN_POINT('Ctrl Pts',(-21.7172848148989,26.2009788506142,26.6344384288426));
#53523=CARTESIAN_POINT('Ctrl Pts',(-21.7187346924914,26.2019808498573,26.6345478031317));
#53524=CARTESIAN_POINT('Ctrl Pts',(-21.7221698010991,26.2043506656441,26.6348065960362));
#53525=CARTESIAN_POINT('Ctrl Pts',(-21.7241557498159,26.2057174472671,26.6349559433114));
#53526=CARTESIAN_POINT('Ctrl Pts',(-21.7300790025364,26.2097841969204,26.6354005874578));
#53527=CARTESIAN_POINT('Ctrl Pts',(-21.7340207966459,26.2124776611459,26.6356954415186));
#53528=CARTESIAN_POINT('Ctrl Pts',(-21.7705143757065,26.2372952839188,26.6384157165108));
#53529=CARTESIAN_POINT('Ctrl Pts',(-21.8034646952323,26.2588313571608,26.640802007203));
#53530=CARTESIAN_POINT('Ctrl Pts',(-21.8436192101301,26.2840383748532,26.6436374568762));
#53531=CARTESIAN_POINT('Ctrl Pts',(-21.8504514119529,26.2882916998571,26.6441174127544));
#53532=CARTESIAN_POINT('Ctrl Pts',(-21.9282636129354,26.3363294741816,26.6495562721621));
#53533=CARTESIAN_POINT('Ctrl Pts',(-22.0008974377762,26.3773658832763,26.6543754537399));
#53534=CARTESIAN_POINT('Ctrl Pts',(-22.0750360239718,26.4155367789973,26.65912344949));
#53535=CARTESIAN_POINT('Origin',(-23.5502525316942,23.5502525316942,-77.3107734492734));
#53536=CARTESIAN_POINT('',(-22.0750359096863,26.4155367201564,28.1544576001758));
#53537=CARTESIAN_POINT('',(-22.0750363456406,26.4155369446113,27.9044917472066));
#53538=CARTESIAN_POINT('',(-22.0750360153461,26.4155367745563,-77.3107734492734));
#53539=CARTESIAN_POINT('Ctrl Pts',(-22.0750359096863,26.4155367201564,28.1544576001758));
#53540=CARTESIAN_POINT('Ctrl Pts',(-22.0173610161786,26.3858422968536,28.1508130336123));
#53541=CARTESIAN_POINT('Ctrl Pts',(-21.9605783308166,26.3544042342411,28.147146887933));
#53542=CARTESIAN_POINT('Ctrl Pts',(-21.8139335814481,26.2673234195051,28.1374047791776));
#53543=CARTESIAN_POINT('Ctrl Pts',(-21.725814651594,26.2089554106126,28.1312676286439));
#53544=CARTESIAN_POINT('Ctrl Pts',(-21.6151963563925,26.1275921543532,28.1230816475099));
#53545=CARTESIAN_POINT('Ctrl Pts',(-21.5899458145721,26.1084392723183,28.1211787550168));
#53546=CARTESIAN_POINT('Ctrl Pts',(-21.5493190360085,26.0766685882533,28.1180582775673));
#53547=CARTESIAN_POINT('Ctrl Pts',(-21.5337695635216,26.064275076638,28.116849559606));
#53548=CARTESIAN_POINT('Ctrl Pts',(-21.5149129043682,26.0489581192546,28.1153656889653));
#53549=CARTESIAN_POINT('Ctrl Pts',(-21.5114954922939,26.0461705483487,28.1150960325726));
#53550=CARTESIAN_POINT('Ctrl Pts',(-21.5048860999888,26.0407566591471,28.1145730798338));
#53551=CARTESIAN_POINT('Ctrl Pts',(-21.5016934280596,26.0381311958314,28.1143198184589));
#53552=CARTESIAN_POINT('Ctrl Pts',(-21.4961708627039,26.0335719287158,28.1138806067314));
#53553=CARTESIAN_POINT('Ctrl Pts',(-21.4938386217162,26.0316409658685,28.1136947723112));
#53554=CARTESIAN_POINT('Ctrl Pts',(-21.4890028942939,26.0276257587959,28.1133087284619));
#53555=CARTESIAN_POINT('Ctrl Pts',(-21.4864998406915,26.0255410005985,28.1131084981407));
#53556=CARTESIAN_POINT('Ctrl Pts',(-21.4804175589649,26.020459514816,28.1126209541279));
#53557=CARTESIAN_POINT('Ctrl Pts',(-21.4768416802161,26.0174588048731,28.1123334773196));
#53558=CARTESIAN_POINT('Ctrl Pts',(-21.4633962231729,26.0061261319661,28.1112493662718));
#53559=CARTESIAN_POINT('Ctrl Pts',(-21.4535703483005,25.9977427169577,28.1104506155047));
#53560=CARTESIAN_POINT('Ctrl Pts',(-21.2931250632783,25.8591758927199,28.097299958417));
#53561=CARTESIAN_POINT('Ctrl Pts',(-21.1548655263839,25.7153959273152,28.0843552146197));
#53562=CARTESIAN_POINT('Ctrl Pts',(-20.9439116789241,25.4509123084033,28.0617143503197));
#53563=CARTESIAN_POINT('Ctrl Pts',(-20.8642081442081,25.3365009864723,28.052243409155));
#53564=CARTESIAN_POINT('Ctrl Pts',(-20.7059727727865,25.0747037153209,28.0315968215798));
#53565=CARTESIAN_POINT('Ctrl Pts',(-20.6309612746357,24.9256190392759,28.0204799171011));
#53566=CARTESIAN_POINT('Ctrl Pts',(-20.5654721316602,24.7656708210194,28.0096487939715));
#53567=CARTESIAN_POINT('Ctrl Pts',(-20.5631499427657,24.7599524032211,28.0092629792111));
#53568=CARTESIAN_POINT('Ctrl Pts',(-20.5598499533574,24.7517586966472,28.0087122209064));
#53569=CARTESIAN_POINT('Ctrl Pts',(-20.5588587876135,24.7492888584753,28.0085464726686));
#53570=CARTESIAN_POINT('Ctrl Pts',(-20.5571598152388,24.7450400520763,28.0082618029513));
#53571=CARTESIAN_POINT('Ctrl Pts',(-20.5564505335901,24.7432616785064,28.0081427914274));
#53572=CARTESIAN_POINT('Ctrl Pts',(-20.5550948643458,24.7398538024068,28.0079149993422));
#53573=CARTESIAN_POINT('Ctrl Pts',(-20.5544482224511,24.7382244069143,28.0078062031804));
#53574=CARTESIAN_POINT('Ctrl Pts',(-20.5529286098187,24.7343861858119,28.0075501959818));
#53575=CARTESIAN_POINT('Ctrl Pts',(-20.5520567492775,24.7321769175348,28.0074030526787));
#53576=CARTESIAN_POINT('Ctrl Pts',(-20.5494905172452,24.7256530513864,28.0069691700418));
#53577=CARTESIAN_POINT('Ctrl Pts',(-20.5478030019938,24.72133573595,28.0066828441839));
#53578=CARTESIAN_POINT('Ctrl Pts',(-20.533254790345,24.6838776446877,28.0042054654805));
#53579=CARTESIAN_POINT('Ctrl Pts',(-20.5209332921916,24.6505281650556,28.002046283905));
#53580=CARTESIAN_POINT('Ctrl Pts',(-20.4622774570331,24.4833087876907,27.99141776957));
#53581=CARTESIAN_POINT('Ctrl Pts',(-20.4242481289722,24.3466755483813,27.9833565032334));
#53582=CARTESIAN_POINT('Ctrl Pts',(-20.3544882634718,24.0120530095176,27.9641479484535));
#53583=CARTESIAN_POINT('Ctrl Pts',(-20.3319837974126,23.8127659183084,27.9531200035869));
#53584=CARTESIAN_POINT('Ctrl Pts',(-20.3270751115492,23.559408322583,27.9385617576426));
#53585=CARTESIAN_POINT('Ctrl Pts',(-20.3273643030219,23.5061211762853,27.9354720028141));
#53586=CARTESIAN_POINT('Ctrl Pts',(-20.3314137106725,23.3721758928065,27.9276089674043));
#53587=CARTESIAN_POINT('Ctrl Pts',(-20.3368840182894,23.2916104316228,27.9227907573503));
#53588=CARTESIAN_POINT('Ctrl Pts',(-20.34638380226,23.2017769897238,27.9172896845966));
#53589=CARTESIAN_POINT('Ctrl Pts',(-20.3474378828565,23.1922185097991,27.916702736562));
#53590=CARTESIAN_POINT('Ctrl Pts',(-20.349049137874,23.1781843463816,27.9158385252525));
#53591=CARTESIAN_POINT('Ctrl Pts',(-20.3495729590479,23.1737048241652,27.9155623163305));
#53592=CARTESIAN_POINT('Ctrl Pts',(-20.3505073497667,23.1658571017385,27.9150777797798));
#53593=CARTESIAN_POINT('Ctrl Pts',(-20.3509138397677,23.1624884152029,27.9148695814567));
#53594=CARTESIAN_POINT('Ctrl Pts',(-20.3517123552837,23.1559576485855,27.9144655484549));
#53595=CARTESIAN_POINT('Ctrl Pts',(-20.3521037518254,23.1527954941931,27.9142697338976));
#53596=CARTESIAN_POINT('Ctrl Pts',(-20.3530475624256,23.1452619625111,27.9138027824446));
#53597=CARTESIAN_POINT('Ctrl Pts',(-20.3536042520764,23.1408911354199,27.913531510425));
#53598=CARTESIAN_POINT('Ctrl Pts',(-20.3556178021786,23.1253364109476,27.912564846354));
#53599=CARTESIAN_POINT('Ctrl Pts',(-20.3571243931712,23.114159135202,27.9118678808545));
#53600=CARTESIAN_POINT('Ctrl Pts',(-20.3804019490563,22.948055789844,27.9014749709444));
#53601=CARTESIAN_POINT('Ctrl Pts',(-20.4133635458321,22.794932862244,27.891419448734));
#53602=CARTESIAN_POINT('Ctrl Pts',(-20.509851285762,22.4653294160291,27.8687168338023));
#53603=CARTESIAN_POINT('Ctrl Pts',(-20.577920443092,22.2907564304879,27.8559823817404));
#53604=CARTESIAN_POINT('Ctrl Pts',(-20.7333658911343,21.9760328111633,27.8323004933322));
#53605=CARTESIAN_POINT('Ctrl Pts',(-20.8171289436563,21.8347150689012,27.8213683440384));
#53606=CARTESIAN_POINT('Ctrl Pts',(-20.9147367392574,21.6954722464665,27.8107145290983));
#53607=CARTESIAN_POINT('Ctrl Pts',(-20.9181866143207,21.690579870545,27.810340374378));
#53608=CARTESIAN_POINT('Ctrl Pts',(-20.9231663215389,21.6835596071443,27.809803768147));
#53609=CARTESIAN_POINT('Ctrl Pts',(-20.9246851219391,21.6814239662281,27.809640564478));
#53610=CARTESIAN_POINT('Ctrl Pts',(-20.9273137239916,21.6777373219396,27.8093589033964));
#53611=CARTESIAN_POINT('Ctrl Pts',(-20.9284222989055,21.676185449057,27.8092403608338));
#53612=CARTESIAN_POINT('Ctrl Pts',(-20.9305580127126,21.6732013080775,27.8090124539186));
#53613=CARTESIAN_POINT('Ctrl Pts',(-20.9315849467733,21.6717689015858,27.808903075653));
#53614=CARTESIAN_POINT('Ctrl Pts',(-20.9340195629084,21.6683788830866,27.808644256483));
#53615=CARTESIAN_POINT('Ctrl Pts',(-20.9354282702975,21.6664220036515,27.808494886956));
#53616=CARTESIAN_POINT('Ctrl Pts',(-20.939633637727,21.6605940017594,27.8080501257668));
#53617=CARTESIAN_POINT('Ctrl Pts',(-20.9424367235006,21.6567274907922,27.8077551772338));
#53618=CARTESIAN_POINT('Ctrl Pts',(-20.9684482954551,21.62101505498,27.8050319194333));
#53619=CARTESIAN_POINT('Ctrl Pts',(-20.9922317156465,21.5895893263304,27.8026428331372));
#53620=CARTESIAN_POINT('Ctrl Pts',(-21.0181911685565,21.5565651050934,27.8001307140675));
#53621=CARTESIAN_POINT('Ctrl Pts',(-21.019797952492,21.5545261164855,27.7999756040536));
#53622=CARTESIAN_POINT('Ctrl Pts',(-21.0222103552994,21.5514724048369,27.7997432889105));
#53623=CARTESIAN_POINT('Ctrl Pts',(-21.0230141213529,21.5504562274523,27.7996659796996));
#53624=CARTESIAN_POINT('Ctrl Pts',(-21.02942089581,21.542366365425,27.7990504956335));
#53625=CARTESIAN_POINT('Ctrl Pts',(-21.0350530374656,21.5353156838306,27.7985139525816));
#53626=CARTESIAN_POINT('Ctrl Pts',(-21.044248001028,21.5239034579703,27.7976451372829));
#53627=CARTESIAN_POINT('Ctrl Pts',(-21.0477927336282,21.5195274798543,27.7973119047323));
#53628=CARTESIAN_POINT('Ctrl Pts',(-21.0550098561774,21.5106655238709,27.7966368317887));
#53629=CARTESIAN_POINT('Ctrl Pts',(-21.0586829178077,21.5061801180543,27.7962950281465));
#53630=CARTESIAN_POINT('Ctrl Pts',(-21.0725631402396,21.4893231095868,27.7950099038778));
#53631=CARTESIAN_POINT('Ctrl Pts',(-21.082850646771,21.4770176780729,27.7940706340535));
#53632=CARTESIAN_POINT('Ctrl Pts',(-21.1163761966167,21.4375189993406,27.7910501156446));
#53633=CARTESIAN_POINT('Ctrl Pts',(-21.1399757378193,21.4106350611374,27.7889855802773));
#53634=CARTESIAN_POINT('Ctrl Pts',(-21.3045125206393,21.229377234183,27.7749623369691));
#53635=CARTESIAN_POINT('Ctrl Pts',(-21.4597350517808,21.0886361698423,27.7635171374815));
#53636=CARTESIAN_POINT('Ctrl Pts',(-21.7346811458177,20.8842340241497,27.7441479573197));
#53637=CARTESIAN_POINT('Ctrl Pts',(-21.8467000964658,20.8113005957623,27.7364715979163));
#53638=CARTESIAN_POINT('Ctrl Pts',(-22.0086697586828,20.7196334306843,27.7254160127077));
#53639=CARTESIAN_POINT('Ctrl Pts',(-22.0550519189111,20.6948617389377,27.7222558005086));
#53640=CARTESIAN_POINT('Ctrl Pts',(-22.1108373437503,20.6667999211204,27.71845375986));
#53641=CARTESIAN_POINT('Ctrl Pts',(-22.1196776606154,20.6624037518002,27.7178512236386));
#53642=CARTESIAN_POINT('Ctrl Pts',(-22.1326360896558,20.6560338048784,27.716967916939));
#53643=CARTESIAN_POINT('Ctrl Pts',(-22.1367384772796,20.6540280181212,27.7166882661768));
#53644=CARTESIAN_POINT('Ctrl Pts',(-22.1439053449168,20.6505427647349,27.7161996883916));
#53645=CARTESIAN_POINT('Ctrl Pts',(-22.1469679381495,20.6490594164859,27.7159908971604));
#53646=CARTESIAN_POINT('Ctrl Pts',(-22.152889720223,20.6462028082142,27.7155871620169));
#53647=CARTESIAN_POINT('Ctrl Pts',(-22.1557485997197,20.6448289125099,27.7153922405319));
#53648=CARTESIAN_POINT('Ctrl Pts',(-22.1625323940824,20.6415811342,27.7149296907984));
#53649=CARTESIAN_POINT('Ctrl Pts',(-22.1664590763048,20.6397109753052,27.7146619333871));
#53650=CARTESIAN_POINT('Ctrl Pts',(-22.1802749010383,20.6331651982858,27.7137197694954));
#53651=CARTESIAN_POINT('Ctrl Pts',(-22.1901839669419,20.6285320259545,27.7130438927294));
#53652=CARTESIAN_POINT('Ctrl Pts',(-22.3219820388685,20.5677231000673,27.704051991083));
#53653=CARTESIAN_POINT('Ctrl Pts',(-22.4472241929496,20.5191718358914,27.6954735262335));
#53654=CARTESIAN_POINT('Ctrl Pts',(-22.8247606641092,20.399318754444,27.6694875057864));
#53655=CARTESIAN_POINT('Ctrl Pts',(-23.0831311363232,20.3508005047192,27.6514620661094));
#53656=CARTESIAN_POINT('Ctrl Pts',(-23.3873861614961,20.3313332468641,27.631140633707));
#53657=CARTESIAN_POINT('Ctrl Pts',(-23.4303536942529,20.3294465200179,27.6282943878418));
#53658=CARTESIAN_POINT('Ctrl Pts',(-23.5185065593216,20.327342318137,27.6225188607451));
#53659=CARTESIAN_POINT('Ctrl Pts',(-23.5636857014011,20.3272138952396,27.6195932056216));
#53660=CARTESIAN_POINT('Ctrl Pts',(-23.6350151184828,20.3285111632754,27.6150434005071));
#53661=CARTESIAN_POINT('Ctrl Pts',(-23.6611695195116,20.329305517197,27.6133898474699));
#53662=CARTESIAN_POINT('Ctrl Pts',(-23.6917163189335,20.3306058135741,27.6114780686054));
#53663=CARTESIAN_POINT('Ctrl Pts',(-23.6961199317306,20.3308023154679,27.6112029407094));
#53664=CARTESIAN_POINT('Ctrl Pts',(-23.7028331974419,20.331115682965,27.6107842468134));
#53665=CARTESIAN_POINT('Ctrl Pts',(-23.705143128232,20.3312259997142,27.6106403135962));
#53666=CARTESIAN_POINT('Ctrl Pts',(-23.7093168767647,20.3314298309001,27.6103804873017));
#53667=CARTESIAN_POINT('Ctrl Pts',(-23.7111807271371,20.3315224776218,27.6102645455232));
#53668=CARTESIAN_POINT('Ctrl Pts',(-23.7149187095161,20.3317115370841,27.6100321983214));
#53669=CARTESIAN_POINT('Ctrl Pts',(-23.7167928302724,20.3318079674524,27.60991579434));
#53670=CARTESIAN_POINT('Ctrl Pts',(-23.7221147324871,20.3320864597307,27.6095854928809));
#53671=CARTESIAN_POINT('Ctrl Pts',(-23.7255623204566,20.3322724259403,27.6093718161414));
#53672=CARTESIAN_POINT('Ctrl Pts',(-23.7401085142803,20.3330805073928,27.6084714883252));
#53673=CARTESIAN_POINT('Ctrl Pts',(-23.751204333428,20.3337545121117,27.6077877293596));
#53674=CARTESIAN_POINT('Ctrl Pts',(-23.7760449367015,20.3353924740859,27.6062632739094));
#53675=CARTESIAN_POINT('Ctrl Pts',(-23.7897875589025,20.3363871975429,27.6054242190391));
#53676=CARTESIAN_POINT('Ctrl Pts',(-23.8073107995806,20.3377685953849,27.6043593759402));
#53677=CARTESIAN_POINT('Ctrl Pts',(-23.811097436386,20.338073842688,27.6041295718724));
#53678=CARTESIAN_POINT('Ctrl Pts',(-23.8206767815296,20.3388631007708,27.6035489588744));
#53679=CARTESIAN_POINT('Ctrl Pts',(-23.8264687634227,20.3393560920179,27.6031985862971));
#53680=CARTESIAN_POINT('Ctrl Pts',(-23.8415725377017,20.3406828378047,27.6022866313876));
#53681=CARTESIAN_POINT('Ctrl Pts',(-23.8508821581294,20.3415414512581,27.601726222468));
#53682=CARTESIAN_POINT('Ctrl Pts',(-23.8691327926678,20.3433048087797,27.6006306976187));
#53683=CARTESIAN_POINT('Ctrl Pts',(-23.8780740075283,20.3442064618725,27.6000954491404));
#53684=CARTESIAN_POINT('Ctrl Pts',(-23.9005681872112,20.3465699134277,27.598752301149));
#53685=CARTESIAN_POINT('Ctrl Pts',(-23.91411597796,20.3480803344396,27.5979464801079));
#53686=CARTESIAN_POINT('Ctrl Pts',(-23.9605332906161,20.3535537123479,27.5951950874469));
#53687=CARTESIAN_POINT('Ctrl Pts',(-23.9933519492917,20.3579372768804,27.5932661104233));
#53688=CARTESIAN_POINT('Ctrl Pts',(-24.3133225590691,20.4057051647797,27.5745696029612));
#53689=CARTESIAN_POINT('Ctrl Pts',(-24.5934418118021,20.4872092651833,27.5589488049468));
#53690=CARTESIAN_POINT('Ctrl Pts',(-24.9611632059889,20.6506009992864,27.5357504841367));
#53691=CARTESIAN_POINT('Ctrl Pts',(-25.0610109701451,20.7013487525684,27.5291635944778));
#53692=CARTESIAN_POINT('Ctrl Pts',(-25.1689566023336,20.763484827109,27.5216239000751));
#53693=CARTESIAN_POINT('Ctrl Pts',(-25.1798663815724,20.7698504383164,27.5208570016011));
#53694=CARTESIAN_POINT('Ctrl Pts',(-25.1989729464373,20.7811497743986,27.5195051678481));
#53695=CARTESIAN_POINT('Ctrl Pts',(-25.2071857585042,20.7860561990795,27.5189212277312));
#53696=CARTESIAN_POINT('Ctrl Pts',(-25.2192241587753,20.7933210007991,27.5180610171292));
#53697=CARTESIAN_POINT('Ctrl Pts',(-25.2230669076351,20.7956509595305,27.5177857890578));
#53698=CARTESIAN_POINT('Ctrl Pts',(-25.2298007130102,20.7997531282996,27.517302362016));
#53699=CARTESIAN_POINT('Ctrl Pts',(-25.2326938757643,20.8015218819111,27.5170942904235));
#53700=CARTESIAN_POINT('Ctrl Pts',(-25.2383046755696,20.804964257461,27.5166900525897));
#53701=CARTESIAN_POINT('Ctrl Pts',(-25.2410226297742,20.8066373574395,27.5164939057583));
#53702=CARTESIAN_POINT('Ctrl Pts',(-25.2475030898378,20.8106398422967,27.5160254438246));
#53703=CARTESIAN_POINT('Ctrl Pts',(-25.2512632851853,20.8129729403424,27.5157529916559));
#53704=CARTESIAN_POINT('Ctrl Pts',(-25.2646853450385,20.8213392968954,27.5147781933944));
#53705=CARTESIAN_POINT('Ctrl Pts',(-25.274319926005,20.8274159723217,27.514074239335));
#53706=CARTESIAN_POINT('Ctrl Pts',(-25.4232505523995,20.9224561399968,27.5031261631887));
#53707=CARTESIAN_POINT('Ctrl Pts',(-25.5555095637881,21.0219400358619,27.4924793441141));
#53708=CARTESIAN_POINT('Ctrl Pts',(-25.7467908793405,21.190302752394,27.4755879542881));
#53709=CARTESIAN_POINT('Ctrl Pts',(-25.8115395459572,21.2522700899586,27.4695708734129));
#53710=CARTESIAN_POINT('Ctrl Pts',(-25.9969384902576,21.445137295342,27.4515018220242));
#53711=CARTESIAN_POINT('Ctrl Pts',(-26.1094244266201,21.5834208997825,27.4393662821745));
#53712=CARTESIAN_POINT('Ctrl Pts',(-26.2393756517925,21.7733297800473,27.4242536878808));
#53713=CARTESIAN_POINT('Ctrl Pts',(-26.2677811100163,21.8170829698717,27.420870665215));
#53714=CARTESIAN_POINT('Ctrl Pts',(-26.3081984171674,21.8827767203016,27.4159564904869));
#53715=CARTESIAN_POINT('Ctrl Pts',(-26.3210360135567,21.9041966155463,27.414379439218));
#53716=CARTESIAN_POINT('Ctrl Pts',(-26.3357897125286,21.9294753602753,27.4125496386335));
#53717=CARTESIAN_POINT('Ctrl Pts',(-26.3379481996208,21.9331907243602,27.4122814890254));
#53718=CARTESIAN_POINT('Ctrl Pts',(-26.341235647428,21.9388754923069,27.4118724157007));
#53719=CARTESIAN_POINT('Ctrl Pts',(-26.3423699580268,21.9408417721234,27.4117311446076));
#53720=CARTESIAN_POINT('Ctrl Pts',(-26.3444230565874,21.9444094357225,27.4114752228268));
#53721=CARTESIAN_POINT('Ctrl Pts',(-26.3453425425081,21.946010404533,27.4113605267506));
#53722=CARTESIAN_POINT('Ctrl Pts',(-26.3472038953457,21.9492577691987,27.4111281788129));
#53723=CARTESIAN_POINT('Ctrl Pts',(-26.3481456808386,21.9509041999708,27.4110105323902));
#53724=CARTESIAN_POINT('Ctrl Pts',(-26.3508473638997,21.9556369758184,27.4106727926805));
#53725=CARTESIAN_POINT('Ctrl Pts',(-26.3526036191034,21.9587254133571,27.4104529365187));
#53726=CARTESIAN_POINT('Ctrl Pts',(-26.3602491030745,21.9722221623054,27.4094944748164));
#53727=CARTESIAN_POINT('Ctrl Pts',(-26.3660855778112,21.982660478623,27.4087592446812));
#53728=CARTESIAN_POINT('Ctrl Pts',(-26.4667435424267,22.1650596659597,27.396012417811));
#53729=CARTESIAN_POINT('Ctrl Pts',(-26.5457268264232,22.3453301348107,27.3849536534753));
#53730=CARTESIAN_POINT('Ctrl Pts',(-26.6596609686117,22.6873438388451,27.3647813075165));
#53731=CARTESIAN_POINT('Ctrl Pts',(-26.6995496853667,22.8467207464071,27.3556752076593));
#53732=CARTESIAN_POINT('Ctrl Pts',(-26.7509715464855,23.1482258749894,27.33815015481));
#53733=CARTESIAN_POINT('Ctrl Pts',(-26.765557540103,23.2894207899487,27.3298267829904));
#53734=CARTESIAN_POINT('Ctrl Pts',(-26.77115519982,23.4407251969664,27.3206059653181));
#53735=CARTESIAN_POINT('Ctrl Pts',(-26.7714679946659,23.4503467133426,27.3200183593341));
#53736=CARTESIAN_POINT('Ctrl Pts',(-26.7718626896692,23.464430231942,27.3191563742683));
#53737=CARTESIAN_POINT('Ctrl Pts',(-26.7719784396549,23.4688912954683,27.318883058537));
#53738=CARTESIAN_POINT('Ctrl Pts',(-26.7721657216574,23.4767377389219,27.3184018415892));
#53739=CARTESIAN_POINT('Ctrl Pts',(-26.7722411847821,23.4801230254457,27.3181940641295));
#53740=CARTESIAN_POINT('Ctrl Pts',(-26.7723776054423,23.4867087052414,27.3177895433338));
#53741=CARTESIAN_POINT('Ctrl Pts',(-26.7724391304131,23.4899090840198,27.317592818056));
#53742=CARTESIAN_POINT('Ctrl Pts',(-26.7725907084634,23.4984564378133,27.3170670296649));
#53743=CARTESIAN_POINT('Ctrl Pts',(-26.7726722205565,23.5038035372304,27.316737698733));
#53744=CARTESIAN_POINT('Ctrl Pts',(-26.7729175804141,23.5230404143155,27.3155514137426));
#53745=CARTESIAN_POINT('Ctrl Pts',(-26.7730049328194,23.5369308613233,27.314692061835));
#53746=CARTESIAN_POINT('Ctrl Pts',(-26.7729902628023,23.6200588915252,27.3095322508042));
#53747=CARTESIAN_POINT('Ctrl Pts',(-26.7707468127409,23.6892733894291,27.3051649806394));
#53748=CARTESIAN_POINT('Ctrl Pts',(-26.7614124245131,23.8335254060318,27.2959054392696));
#53749=CARTESIAN_POINT('Ctrl Pts',(-26.7539149434557,23.9084942640823,27.291003542779));
#53750=CARTESIAN_POINT('Ctrl Pts',(-26.7211484207959,24.1502302494961,27.2749201630473));
#53751=CARTESIAN_POINT('Ctrl Pts',(-26.6854189927194,24.3152865231714,27.2634913702863));
#53752=CARTESIAN_POINT('Ctrl Pts',(-26.5840181879805,24.6531015103468,27.2396312858963));
#53753=CARTESIAN_POINT('Ctrl Pts',(-26.5160718575201,24.824592907168,27.2272485170435));
#53754=CARTESIAN_POINT('Ctrl Pts',(-26.429043892908,24.9989737949812,27.2149755206588));
#53755=CARTESIAN_POINT('Ctrl Pts',(-26.4241979864778,25.0085633801799,27.2143017286782));
#53756=CARTESIAN_POINT('Ctrl Pts',(-26.4177524192232,25.0211616260647,27.2134182054145));
#53757=CARTESIAN_POINT('Ctrl Pts',(-26.4161958900738,25.024192094803,27.2132058041464));
#53758=CARTESIAN_POINT('Ctrl Pts',(-26.4137787751932,25.0288797673819,27.2128774560556));
#53759=CARTESIAN_POINT('Ctrl Pts',(-26.4129215556488,25.0305386893874,27.2127612965089));
#53760=CARTESIAN_POINT('Ctrl Pts',(-26.4112042771354,25.033854957963,27.2125291685302));
#53761=CARTESIAN_POINT('Ctrl Pts',(-26.4103442250899,25.035512291591,27.2124132012404));
#53762=CARTESIAN_POINT('Ctrl Pts',(-26.4084081121296,25.0392352936305,27.2121527850952));
#53763=CARTESIAN_POINT('Ctrl Pts',(-26.407331254245,25.0413005391533,27.2120083879907));
#53764=CARTESIAN_POINT('Ctrl Pts',(-26.4041307961566,25.0474223213986,27.2115805473663));
#53765=CARTESIAN_POINT('Ctrl Pts',(-26.4020007773195,25.0514755237118,27.211297510813));
#53766=CARTESIAN_POINT('Ctrl Pts',(-26.3848977006121,25.0838531284887,27.2090383392424));
#53767=CARTESIAN_POINT('Ctrl Pts',(-26.3695109845738,25.1119586469161,27.207088091149));
#53768=CARTESIAN_POINT('Ctrl Pts',(-26.3137732135825,25.2102603505334,27.2002887383748));
#53769=CARTESIAN_POINT('Ctrl Pts',(-26.271196233903,25.2791654968496,27.195562271471));
#53770=CARTESIAN_POINT('Ctrl Pts',(-26.0581104338111,25.5966105380004,27.1736255207598));
#53771=CARTESIAN_POINT('Ctrl Pts',(-25.8558943945743,25.8220285277798,27.1574130288819));
#53772=CARTESIAN_POINT('Ctrl Pts',(-25.5508969995853,26.0786895964007,27.134194091959));
#53773=CARTESIAN_POINT('Ctrl Pts',(-25.4737104300391,26.1378922087295,27.128418552256));
#53774=CARTESIAN_POINT('Ctrl Pts',(-25.3863341453027,26.1988386784496,27.1219340124906));
#53775=CARTESIAN_POINT('Ctrl Pts',(-25.3786738902483,26.2041326347396,27.1213659687162));
#53776=CARTESIAN_POINT('Ctrl Pts',(-25.3672644135931,26.2119448092281,27.1205205318743));
#53777=CARTESIAN_POINT('Ctrl Pts',(-25.3635326206346,26.2144884968369,27.1202441071993));
#53778=CARTESIAN_POINT('Ctrl Pts',(-25.3571342981806,26.2188300904842,27.1197703296585));
#53779=CARTESIAN_POINT('Ctrl Pts',(-25.3544703940264,26.2206318700031,27.1195731238541));
#53780=CARTESIAN_POINT('Ctrl Pts',(-25.3492819864506,26.2241298350871,27.1191891244928));
#53781=CARTESIAN_POINT('Ctrl Pts',(-25.3467577697609,26.2258264406309,27.1190023471373));
#53782=CARTESIAN_POINT('Ctrl Pts',(-25.3407135827587,26.22987651953,27.1185552119227));
#53783=CARTESIAN_POINT('Ctrl Pts',(-25.3371913754047,26.2322266292812,27.1182947275467));
#53784=CARTESIAN_POINT('Ctrl Pts',(-25.3266128682736,26.2392547988692,27.1175126297482));
#53785=CARTESIAN_POINT('Ctrl Pts',(-25.3195427970398,26.2439119743493,27.1169902319159));
#53786=CARTESIAN_POINT('Ctrl Pts',(-25.2599330235087,26.2828420050913,27.1125882183764));
#53787=CARTESIAN_POINT('Ctrl Pts',(-25.2064245119428,26.3155999043005,27.108652448068));
#53788=CARTESIAN_POINT('Ctrl Pts',(-25.0686461137499,26.3945143045002,27.0985466777094));
#53789=CARTESIAN_POINT('Ctrl Pts',(-24.9832097687096,26.4385002248896,27.092304654803));
#53790=CARTESIAN_POINT('Ctrl Pts',(-24.5989328247726,26.6150904433102,27.0643679070284));
#53791=CARTESIAN_POINT('Ctrl Pts',(-24.2829231040249,26.70558639212,27.0415193935694));
#53792=CARTESIAN_POINT('Ctrl Pts',(-23.9303606208478,26.7506358029833,27.0188044626008));
#53793=CARTESIAN_POINT('Ctrl Pts',(-23.9019479288539,26.7538826178576,27.0169946942335));
#53794=CARTESIAN_POINT('Ctrl Pts',(-23.8687573883957,26.7572285041729,27.0149077710829));
#53795=CARTESIAN_POINT('Ctrl Pts',(-23.8640190807496,26.7576955608353,27.014610485272));
#53796=CARTESIAN_POINT('Ctrl Pts',(-23.8569168585411,26.7583797405284,27.0141658693321));
#53797=CARTESIAN_POINT('Ctrl Pts',(-23.8545537378389,26.758604752609,27.0140180955647));
#53798=CARTESIAN_POINT('Ctrl Pts',(-23.8503229984115,26.7590028796378,27.0137538281405));
#53799=CARTESIAN_POINT('Ctrl Pts',(-23.8484554780954,26.7591769750633,27.0136372788856));
#53800=CARTESIAN_POINT('Ctrl Pts',(-23.8445054264257,26.7595417317612,27.0133909801908));
#53801=CARTESIAN_POINT('Ctrl Pts',(-23.8424228664763,26.7597319959154,27.0132612537576));
#53802=CARTESIAN_POINT('Ctrl Pts',(-23.8369422067294,26.7602273342159,27.0129201869163));
#53803=CARTESIAN_POINT('Ctrl Pts',(-23.8335437935575,26.7605290406268,27.012709037505));
#53804=CARTESIAN_POINT('Ctrl Pts',(-23.8180641847547,26.7618785269774,27.0117487714541));
#53805=CARTESIAN_POINT('Ctrl Pts',(-23.805977405847,26.7628635281993,27.0110031633054));
#53806=CARTESIAN_POINT('Ctrl Pts',(-23.618824813142,26.7770524431776,26.9995188975899));
#53807=CARTESIAN_POINT('Ctrl Pts',(-23.4429438948042,26.7759995369787,26.9895416721648));
#53808=CARTESIAN_POINT('Ctrl Pts',(-23.0261258103459,26.7393534901486,26.9660607821395));
#53809=CARTESIAN_POINT('Ctrl Pts',(-22.7874472796697,26.6908248460841,26.9526936196271));
#53810=CARTESIAN_POINT('Ctrl Pts',(-22.5374643231404,26.6097912895227,26.9372947586525));
#53811=CARTESIAN_POINT('Ctrl Pts',(-22.5185016901403,26.603448814755,26.936118128442));
#53812=CARTESIAN_POINT('Ctrl Pts',(-22.4947877294154,26.5952710080177,26.9346353341244));
#53813=CARTESIAN_POINT('Ctrl Pts',(-22.4899798299442,26.5936002389918,26.9343341165775));
#53814=CARTESIAN_POINT('Ctrl Pts',(-22.4813158115808,26.5905664264087,26.9337902370704));
#53815=CARTESIAN_POINT('Ctrl Pts',(-22.4774582845578,26.5892074166991,26.9335476978937));
#53816=CARTESIAN_POINT('Ctrl Pts',(-22.4704504416563,26.5867235423681,26.9331063781281));
#53817=CARTESIAN_POINT('Ctrl Pts',(-22.4672992662039,26.5856011075513,26.9329076722053));
#53818=CARTESIAN_POINT('Ctrl Pts',(-22.4143817481995,26.5666592264092,26.9295664054233));
#53819=CARTESIAN_POINT('Ctrl Pts',(-22.3650618775877,26.5476237798608,26.9263865334187));
#53820=CARTESIAN_POINT('Ctrl Pts',(-22.308170626901,26.524042420502,26.9226334945939));
#53821=CARTESIAN_POINT('Ctrl Pts',(-22.300120411541,26.5206672234149,26.9221004281876));
#53822=CARTESIAN_POINT('Ctrl Pts',(-22.2881369025134,26.5155855792361,26.9213038793064));
#53823=CARTESIAN_POINT('Ctrl Pts',(-22.2841930943073,26.5139039020461,26.9210412418666));
#53824=CARTESIAN_POINT('Ctrl Pts',(-22.2771623002621,26.5108893097006,26.9205721457793));
#53825=CARTESIAN_POINT('Ctrl Pts',(-22.2740740168574,26.5095594212859,26.9203657908202));
#53826=CARTESIAN_POINT('Ctrl Pts',(-22.267564697252,26.5067442687712,26.9199302025796));
#53827=CARTESIAN_POINT('Ctrl Pts',(-22.2641441488214,26.5052578953692,26.9197009315541));
#53828=CARTESIAN_POINT('Ctrl Pts',(-22.2551098863997,26.5013134674819,26.9190943880917));
#53829=CARTESIAN_POINT('Ctrl Pts',(-22.2495006102249,26.4988453412148,26.918716770635));
#53830=CARTESIAN_POINT('Ctrl Pts',(-22.2245072635091,26.4877628714342,26.9170296228426));
#53831=CARTESIAN_POINT('Ctrl Pts',(-22.2052018370598,26.4789734310645,26.9157140811468));
#53832=CARTESIAN_POINT('Ctrl Pts',(-22.148648067492,26.4525483281695,26.9118231005602));
#53833=CARTESIAN_POINT('Ctrl Pts',(-22.1116584725339,26.4343921662557,26.9092301670837));
#53834=CARTESIAN_POINT('Ctrl Pts',(-22.0750359502314,26.4155367410314,26.9066135500179));
#53835=CARTESIAN_POINT('Ctrl Pts',(-22.0750360239718,26.4155367789973,26.65912344949));
#53836=CARTESIAN_POINT('Ctrl Pts',(-22.1002035109265,26.4284944784815,26.6607352299033));
#53837=CARTESIAN_POINT('Ctrl Pts',(-22.1255444033382,26.4411219678302,26.662338762767));
#53838=CARTESIAN_POINT('Ctrl Pts',(-22.318005719262,26.5338800785094,26.6743948788536));
#53839=CARTESIAN_POINT('Ctrl Pts',(-22.4915870603914,26.5997924768428,26.6845988913205));
#53840=CARTESIAN_POINT('Ctrl Pts',(-22.7833682994856,26.6826519796707,26.7018404289965));
#53841=CARTESIAN_POINT('Ctrl Pts',(-22.8985383847735,26.70862272329,26.7086625340796));
#53842=CARTESIAN_POINT('Ctrl Pts',(-23.0655028963066,26.7367509679445,26.7187404833921));
#53843=CARTESIAN_POINT('Ctrl Pts',(-23.1163346709547,26.7440698909521,26.7218325006049));
#53844=CARTESIAN_POINT('Ctrl Pts',(-23.1752450752332,26.7511197136806,26.7254502496706));
#53845=CARTESIAN_POINT('Ctrl Pts',(-23.1831761009048,26.7520389395093,26.7259380139693));
#53846=CARTESIAN_POINT('Ctrl Pts',(-23.1952194946412,26.7533894632106,26.7266797989716));
#53847=CARTESIAN_POINT('Ctrl Pts',(-23.1993294522773,26.7538423386956,26.7269331377892));
#53848=CARTESIAN_POINT('Ctrl Pts',(-23.2067686647732,26.7546475765935,26.7273920505936));
#53849=CARTESIAN_POINT('Ctrl Pts',(-23.2100976239146,26.755002663793,26.7275975382357));
#53850=CARTESIAN_POINT('Ctrl Pts',(-23.2167439333816,26.7557011274602,26.728008058016));
#53851=CARTESIAN_POINT('Ctrl Pts',(-23.2200612755955,26.7560445429623,26.7282130886588));
#53852=CARTESIAN_POINT('Ctrl Pts',(-23.2293689523761,26.7569934850396,26.7287887232825));
#53853=CARTESIAN_POINT('Ctrl Pts',(-23.2353604364257,26.7575873724753,26.7291596940361));
#53854=CARTESIAN_POINT('Ctrl Pts',(-23.2597971155129,26.7599404501934,26.7306744884708));
#53855=CARTESIAN_POINT('Ctrl Pts',(-23.2782553686142,26.7615573137323,26.7318227896483));
#53856=CARTESIAN_POINT('Ctrl Pts',(-23.6010348871531,26.7870285710069,26.7519775486845));
#53857=CARTESIAN_POINT('Ctrl Pts',(-23.907145919701,26.7676794194904,26.7724722575359));
#53858=CARTESIAN_POINT('Ctrl Pts',(-24.3923106645748,26.6668716828463,26.8059986069167));
#53859=CARTESIAN_POINT('Ctrl Pts',(-24.5749737445106,26.6116807711367,26.8188149936768));
#53860=CARTESIAN_POINT('Ctrl Pts',(-24.7566209284287,26.5387004286289,26.8311046322034));
#53861=CARTESIAN_POINT('Ctrl Pts',(-24.7615242857119,26.5367163737968,26.831436007984));
#53862=CARTESIAN_POINT('Ctrl Pts',(-24.7703200395528,26.5331321051258,26.8320297453242));
#53863=CARTESIAN_POINT('Ctrl Pts',(-24.774214214319,26.5315363278589,26.8322923685132));
#53864=CARTESIAN_POINT('Ctrl Pts',(-24.7800692257252,26.5291236221627,26.8326868504849));
#53865=CARTESIAN_POINT('Ctrl Pts',(-24.7820323792746,26.5283123836286,26.8328190537518));
#53866=CARTESIAN_POINT('Ctrl Pts',(-24.7856880139195,26.5267975240134,26.8330651106059));
#53867=CARTESIAN_POINT('Ctrl Pts',(-24.7873806942676,26.5260944010596,26.833178994207));
#53868=CARTESIAN_POINT('Ctrl Pts',(-24.7907828867047,26.5246777589073,26.83340779506));
#53869=CARTESIAN_POINT('Ctrl Pts',(-24.7924923770923,26.5239642124949,26.8335227100362));
#53870=CARTESIAN_POINT('Ctrl Pts',(-24.7972755919546,26.5219628399031,26.8338441088757));
#53871=CARTESIAN_POINT('Ctrl Pts',(-24.8003479468294,26.5206717145762,26.834050390926));
#53872=CARTESIAN_POINT('Ctrl Pts',(-24.8127906126895,26.5154200892518,26.8348851856375));
#53873=CARTESIAN_POINT('Ctrl Pts',(-24.8221442813769,26.5114199423619,26.8355113029031));
#53874=CARTESIAN_POINT('Ctrl Pts',(-24.9825994218186,26.441899880304,26.8462298049572));
#53875=CARTESIAN_POINT('Ctrl Pts',(-25.1285027578106,26.3649256424062,26.8556443693302));
#53876=CARTESIAN_POINT('Ctrl Pts',(-25.3542985523088,26.2226975422164,26.8706580084505));
#53877=CARTESIAN_POINT('Ctrl Pts',(-25.4380638258682,26.1641984615646,26.8763371310586));
#53878=CARTESIAN_POINT('Ctrl Pts',(-25.6105116033297,26.0311466486744,26.8885350775715));
#53879=CARTESIAN_POINT('Ctrl Pts',(-25.6982355750633,25.9555944076823,26.8950573080001));
#53880=CARTESIAN_POINT('Ctrl Pts',(-25.8412359759228,25.8183619840093,26.9064954835451));
#53881=CARTESIAN_POINT('Ctrl Pts',(-25.8985483084863,25.7589695692253,26.9113303768721));
#53882=CARTESIAN_POINT('Ctrl Pts',(-25.981860334445,25.665721971269,26.9188056440167));
#53883=CARTESIAN_POINT('Ctrl Pts',(-26.009572927011,25.6334400857977,26.921373735971));
#53884=CARTESIAN_POINT('Ctrl Pts',(-26.0414713526595,25.5947583587771,26.9244318731567));
#53885=CARTESIAN_POINT('Ctrl Pts',(-26.0462844998661,25.5888794478346,26.9248961432663));
#53886=CARTESIAN_POINT('Ctrl Pts',(-26.053633289723,25.579838393628,26.9256093774157));
#53887=CARTESIAN_POINT('Ctrl Pts',(-26.0561838539742,25.5766883679369,26.9258577377227));
#53888=CARTESIAN_POINT('Ctrl Pts',(-26.060827291813,25.5709314058864,26.9263113877445));
#53889=CARTESIAN_POINT('Ctrl Pts',(-26.0629220672863,25.5683260049665,26.9265166004236));
#53890=CARTESIAN_POINT('Ctrl Pts',(-26.067128091261,25.5630780136564,26.926929769404));
#53891=CARTESIAN_POINT('Ctrl Pts',(-26.069239240876,25.5604353497501,26.9271377293122));
#53892=CARTESIAN_POINT('Ctrl Pts',(-26.0752430314933,25.5528957030038,26.9277307838726));
#53893=CARTESIAN_POINT('Ctrl Pts',(-26.0791255640723,25.5479907229734,26.9281162827488));
#53894=CARTESIAN_POINT('Ctrl Pts',(-26.0956105400957,25.5270394391697,26.9297615941946));
#53895=CARTESIAN_POINT('Ctrl Pts',(-26.1080745064524,25.5108852313878,26.9310269051937));
#53896=CARTESIAN_POINT('Ctrl Pts',(-26.3373474263915,25.2078235103166,26.9547080494624));
#53897=CARTESIAN_POINT('Ctrl Pts',(-26.5047361887244,24.88678646575,26.9792812596588));
#53898=CARTESIAN_POINT('Ctrl Pts',(-26.6436713915966,24.4586087445473,27.0094934229028));
#53899=CARTESIAN_POINT('Ctrl Pts',(-26.6680217453622,24.3711477301968,27.0155171421788));
#53900=CARTESIAN_POINT('Ctrl Pts',(-26.699409123468,24.23667157406,27.024449247208));
#53901=CARTESIAN_POINT('Ctrl Pts',(-26.7091523593242,24.190339102167,27.0274681427176));
#53902=CARTESIAN_POINT('Ctrl Pts',(-26.7187884775357,24.1389139732259,27.0307419454235));
#53903=CARTESIAN_POINT('Ctrl Pts',(-26.719693792244,24.1340199764464,27.0310527383684));
#53904=CARTESIAN_POINT('Ctrl Pts',(-26.7210206236057,24.1267532489419,27.0315130543606));
#53905=CARTESIAN_POINT('Ctrl Pts',(-26.7214508165439,24.1243821406925,27.0316630712046));
#53906=CARTESIAN_POINT('Ctrl Pts',(-26.7221801271835,24.1203365472595,27.0319187162889));
#53907=CARTESIAN_POINT('Ctrl Pts',(-26.7224805787188,24.1186623077846,27.0320244213522));
#53908=CARTESIAN_POINT('Ctrl Pts',(-26.7230945802085,24.1152251891701,27.0322412386783));
#53909=CARTESIAN_POINT('Ctrl Pts',(-26.7234079858506,24.1134622904095,27.0323523424115));
#53910=CARTESIAN_POINT('Ctrl Pts',(-26.7241584136641,24.1092206435285,27.0326194219322));
#53911=CARTESIAN_POINT('Ctrl Pts',(-26.7245940023249,24.1067416381333,27.0327753152882));
#53912=CARTESIAN_POINT('Ctrl Pts',(-26.7261706111393,24.0977068180355,27.0333427548533));
#53913=CARTESIAN_POINT('Ctrl Pts',(-26.7272942403617,24.0911479247513,27.0337533126045));
#53914=CARTESIAN_POINT('Ctrl Pts',(-26.7291805479057,24.0799284062761,27.0344533208118));
#53915=CARTESIAN_POINT('Ctrl Pts',(-26.7299533057075,24.0752695340414,27.0347433246901));
#53916=CARTESIAN_POINT('Ctrl Pts',(-26.758704891206,23.8995373632741,27.0456574646504));
#53917=CARTESIAN_POINT('Ctrl Pts',(-26.7728503665737,23.7264580187519,27.055528652753));
#53918=CARTESIAN_POINT('Ctrl Pts',(-26.7732154882093,23.3070170739045,27.0790849247666));
#53919=CARTESIAN_POINT('Ctrl Pts',(-26.7452551395816,23.0617801032081,27.0926117794247));
#53920=CARTESIAN_POINT('Ctrl Pts',(-26.6850037036113,22.8020019501826,27.1082309318386));
#53921=CARTESIAN_POINT('Ctrl Pts',(-26.6801457921284,22.781934892698,27.1094454763104));
#53922=CARTESIAN_POINT('Ctrl Pts',(-26.673966630763,22.7574416553488,27.1109383850029));
#53923=CARTESIAN_POINT('Ctrl Pts',(-26.6728281846266,22.7529695519551,27.1112113965384));
#53924=CARTESIAN_POINT('Ctrl Pts',(-26.6706819518144,22.7446137196177,27.1117223124583));
#53925=CARTESIAN_POINT('Ctrl Pts',(-26.6696765090945,22.7407293939822,27.1119601473094));
#53926=CARTESIAN_POINT('Ctrl Pts',(-26.667404338373,22.7320184100123,27.1124942606677));
#53927=CARTESIAN_POINT('Ctrl Pts',(-26.6661336504255,22.7271928028153,27.1127906564237));
#53928=CARTESIAN_POINT('Ctrl Pts',(-26.6630711588772,22.7156713180635,27.1134995672237));
#53929=CARTESIAN_POINT('Ctrl Pts',(-26.6612689557792,22.7089782506919,27.1139123938956));
#53930=CARTESIAN_POINT('Ctrl Pts',(-26.6589095236445,22.7003269976165,27.1144473255561));
#53931=CARTESIAN_POINT('Ctrl Pts',(-26.6583720029826,22.6983634196324,27.1145688275838));
#53932=CARTESIAN_POINT('Ctrl Pts',(-26.6565839608661,22.6918558715591,27.1149717953353));
#53933=CARTESIAN_POINT('Ctrl Pts',(-26.6553253364479,22.6873141498702,27.115253509239));
#53934=CARTESIAN_POINT('Ctrl Pts',(-26.6535525573608,22.680971206753,27.1156476224777));
#53935=CARTESIAN_POINT('Ctrl Pts',(-26.6530467838057,22.6791676332855,27.115759762084));
#53936=CARTESIAN_POINT('Ctrl Pts',(-26.6510969700594,22.6722378994951,27.116190921518));
#53937=CARTESIAN_POINT('Ctrl Pts',(-26.6496418021535,22.6671149008844,27.116510286515));
#53938=CARTESIAN_POINT('Ctrl Pts',(-26.644749645636,22.6500528154092,27.1175760139364));
#53939=CARTESIAN_POINT('Ctrl Pts',(-26.6412563476154,22.6381301052484,27.1183241364571));
#53940=CARTESIAN_POINT('Ctrl Pts',(-26.6311913943934,22.6045000924015,27.1204442316431));
#53941=CARTESIAN_POINT('Ctrl Pts',(-26.6244595045691,22.582841864368,27.1218212939463));
#53942=CARTESIAN_POINT('Ctrl Pts',(-26.6154995748848,22.5550537543438,27.1236037830363));
#53943=CARTESIAN_POINT('Ctrl Pts',(-26.613480641613,22.5488567119275,27.124002305748));
#53944=CARTESIAN_POINT('Ctrl Pts',(-26.6102496316203,22.5390404477968,27.124635191442));
#53945=CARTESIAN_POINT('Ctrl Pts',(-26.6090498926251,22.5354171584736,27.1248691462837));
#53946=CARTESIAN_POINT('Ctrl Pts',(-26.6067954898645,22.5286490324378,27.1253068201278));
#53947=CARTESIAN_POINT('Ctrl Pts',(-26.6057424010411,22.5255036731826,27.125510486748));
#53948=CARTESIAN_POINT('Ctrl Pts',(-26.6033660899418,22.5184423511547,27.1259683179138));
#53949=CARTESIAN_POINT('Ctrl Pts',(-26.602040187684,22.5145273023432,27.1262225710365));
#53950=CARTESIAN_POINT('Ctrl Pts',(-26.5981332111613,22.5030636424175,27.1269682735413));
#53951=CARTESIAN_POINT('Ctrl Pts',(-26.5955316493111,22.4955220921668,27.1274604024123));
#53952=CARTESIAN_POINT('Ctrl Pts',(-26.5760303630848,22.4396643380187,27.1311171033311));
#53953=CARTESIAN_POINT('Ctrl Pts',(-26.5580105050036,22.3917495719368,27.1343188426746));
#53954=CARTESIAN_POINT('Ctrl Pts',(-26.4949394301051,22.2354478697928,27.1449874608855));
#53955=CARTESIAN_POINT('Ctrl Pts',(-26.4451130206286,22.1291017253764,27.152611931003));
#53956=CARTESIAN_POINT('Ctrl Pts',(-26.2409640086401,21.7488866174755,27.1811994800256));
#53957=CARTESIAN_POINT('Ctrl Pts',(-26.0526558250693,21.4953051377525,27.2031124456538));
#53958=CARTESIAN_POINT('Ctrl Pts',(-25.8264313261303,21.2687698535442,27.2236225025693));
#53959=CARTESIAN_POINT('Ctrl Pts',(-25.8222063003646,21.2645624413434,27.2240037393628));
#53960=CARTESIAN_POINT('Ctrl Pts',(-25.8156028846158,21.2580229542619,27.2245967305327));
#53961=CARTESIAN_POINT('Ctrl Pts',(-25.8132325368919,21.2556828218254,27.2248090193358));
#53962=CARTESIAN_POINT('Ctrl Pts',(-25.8074681233114,21.2500095086516,27.2253238897863));
#53963=CARTESIAN_POINT('Ctrl Pts',(-25.8040702859314,21.2466801487692,27.2256262134075));
#53964=CARTESIAN_POINT('Ctrl Pts',(-25.7961954063491,21.2389980767049,27.2263241633312));
#53965=CARTESIAN_POINT('Ctrl Pts',(-25.7917130421661,21.2346508100302,27.2267194129556));
#53966=CARTESIAN_POINT('Ctrl Pts',(-25.7773228895002,21.2207753085499,27.2279817809126));
#53967=CARTESIAN_POINT('Ctrl Pts',(-25.7673665936322,21.2112972597313,27.2288453213514));
#53968=CARTESIAN_POINT('Ctrl Pts',(-25.7546509633859,21.1993465714761,27.2299353752249));
#53969=CARTESIAN_POINT('Ctrl Pts',(-25.7519477914895,21.1968147775232,27.2301663777779));
#53970=CARTESIAN_POINT('Ctrl Pts',(-25.7476591923194,21.1928119263383,27.2305317043135));
#53971=CARTESIAN_POINT('Ctrl Pts',(-25.7460766489504,21.1913378053671,27.2306662646679));
#53972=CARTESIAN_POINT('Ctrl Pts',(-25.7432629046183,21.1887221199188,27.2309050668521));
#53973=CARTESIAN_POINT('Ctrl Pts',(-25.742032302393,21.1875799309568,27.2310093570647));
#53974=CARTESIAN_POINT('Ctrl Pts',(-25.7391715037881,21.1849288264872,27.2312514521635));
#53975=CARTESIAN_POINT('Ctrl Pts',(-25.7375406422634,21.1834206368945,27.2313892006504));
#53976=CARTESIAN_POINT('Ctrl Pts',(-25.7329175121721,21.1791541137674,27.2317789468384));
#53977=CARTESIAN_POINT('Ctrl Pts',(-25.7299215627231,21.176399747694,27.2320306395743));
#53978=CARTESIAN_POINT('Ctrl Pts',(-25.7117197351977,21.1597291644794,27.2335545463208));
#53979=CARTESIAN_POINT('Ctrl Pts',(-25.6963853993515,21.145953006266,27.2348162232521));
#53980=CARTESIAN_POINT('Ctrl Pts',(-25.6500887074748,21.1051565766362,27.2385634401385));
#53981=CARTESIAN_POINT('Ctrl Pts',(-25.618739539945,21.078579406316,27.2410192488098));
#53982=CARTESIAN_POINT('Ctrl Pts',(-25.5263522252921,21.0032446822363,27.2480526939295));
#53983=CARTESIAN_POINT('Ctrl Pts',(-25.464036723143,20.9560955162728,27.2525470872287));
#53984=CARTESIAN_POINT('Ctrl Pts',(-25.1058498441037,20.7050233856249,27.2773907496014));
#53985=CARTESIAN_POINT('Ctrl Pts',(-24.7792507677546,20.5494557495119,27.2967378105584));
#53986=CARTESIAN_POINT('Ctrl Pts',(-24.4140977229529,20.4453684886603,27.3196999507841));
#53987=CARTESIAN_POINT('Ctrl Pts',(-24.3944337164012,20.4399645172474,27.3209391269503));
#53988=CARTESIAN_POINT('Ctrl Pts',(-24.3686738602927,20.4331475914606,27.3225663040356));
#53989=CARTESIAN_POINT('Ctrl Pts',(-24.362623017741,20.4315651680647,27.3229487950949));
#53990=CARTESIAN_POINT('Ctrl Pts',(-24.3532930672447,20.4291541834139,27.3235390065003));
#53991=CARTESIAN_POINT('Ctrl Pts',(-24.3500171737522,20.4283131475052,27.3237463222452));
#53992=CARTESIAN_POINT('Ctrl Pts',(-24.3435654315749,20.4266675818825,27.3241547885204));
#53993=CARTESIAN_POINT('Ctrl Pts',(-24.3403896674157,20.4258627348802,27.3243559284966));
#53994=CARTESIAN_POINT('Ctrl Pts',(-24.333388687487,20.424099804423,27.3247995188891));
#53995=CARTESIAN_POINT('Ctrl Pts',(-24.3295629336645,20.423143897525,27.3250420393965));
#53996=CARTESIAN_POINT('Ctrl Pts',(-24.3216346509618,20.4211783812999,27.3255448700825));
#53997=CARTESIAN_POINT('Ctrl Pts',(-24.3175318738928,20.4201698134016,27.325805213452));
#53998=CARTESIAN_POINT('Ctrl Pts',(-24.3070366382876,20.4176116899691,27.326471544544));
#53999=CARTESIAN_POINT('Ctrl Pts',(-24.3006414202909,20.4160736372982,27.3268779032427));
#54000=CARTESIAN_POINT('Ctrl Pts',(-24.2821957166974,20.4116971302992,27.3280509444554));
#54001=CARTESIAN_POINT('Ctrl Pts',(-24.2701336260797,20.4089085459533,27.32881923142));
#54002=CARTESIAN_POINT('Ctrl Pts',(-24.1524395267564,20.3824128043248,27.336327877405));
#54003=CARTESIAN_POINT('Ctrl Pts',(-24.0457037103836,20.363975494389,27.343236621469));
#54004=CARTESIAN_POINT('Ctrl Pts',(-23.6481260920866,20.3157588418114,27.3693579170136));
#54005=CARTESIAN_POINT('Ctrl Pts',(-23.3546184897718,20.3202038204604,27.38955007316));
#54006=CARTESIAN_POINT('Ctrl Pts',(-23.0375823867764,20.3684135808812,27.410819513959));
#54007=CARTESIAN_POINT('Ctrl Pts',(-23.0094640476387,20.3730717548855,27.4126995840299));
#54008=CARTESIAN_POINT('Ctrl Pts',(-22.971415572815,20.3798947525046,27.4152319490993));
#54009=CARTESIAN_POINT('Ctrl Pts',(-22.9614290834225,20.3817343252777,27.4158955176354));
#54010=CARTESIAN_POINT('Ctrl Pts',(-22.9475756134337,20.3843539778636,27.4168143663633));
#54011=CARTESIAN_POINT('Ctrl Pts',(-22.9437012138919,20.3850939858912,27.4170711593587));
#54012=CARTESIAN_POINT('Ctrl Pts',(-22.9372451691874,20.3863393760984,27.4174987494476));
#54013=CARTESIAN_POINT('Ctrl Pts',(-22.9346627761465,20.3868408076865,27.4176697003247));
#54014=CARTESIAN_POINT('Ctrl Pts',(-22.9227430016417,20.3891704572956,27.4184583788062));
#54015=CARTESIAN_POINT('Ctrl Pts',(-22.9134130305478,20.3910368781875,27.4190745842761));
#54016=CARTESIAN_POINT('Ctrl Pts',(-22.9011913622054,20.3935381127195,27.4198801917714));
#54017=CARTESIAN_POINT('Ctrl Pts',(-22.8982921773616,20.3941356103474,27.4200711784609));
#54018=CARTESIAN_POINT('Ctrl Pts',(-22.889751807307,20.3959079787457,27.4206334312569));
#54019=CARTESIAN_POINT('Ctrl Pts',(-22.8841129136074,20.3970939920961,27.4210042126531));
#54020=CARTESIAN_POINT('Ctrl Pts',(-22.8436380890675,20.4057203742661,27.4236622027573));
#54021=CARTESIAN_POINT('Ctrl Pts',(-22.8089226567796,20.4137231218494,27.4259238714752));
#54022=CARTESIAN_POINT('Ctrl Pts',(-22.7698429148051,20.4234170849069,27.4284438554017));
#54023=CARTESIAN_POINT('Ctrl Pts',(-22.7653429015337,20.4245436593678,27.4287336382437));
#54024=CARTESIAN_POINT('Ctrl Pts',(-22.7585414664707,20.4262620070365,27.4291710136679));
#54025=CARTESIAN_POINT('Ctrl Pts',(-22.7562382652036,20.4268466096842,27.4293190182633));
#54026=CARTESIAN_POINT('Ctrl Pts',(-22.7522365205823,20.427867052053,27.4295759853162));
#54027=CARTESIAN_POINT('Ctrl Pts',(-22.750537686657,20.4283017306523,27.429685015341));
#54028=CARTESIAN_POINT('Ctrl Pts',(-22.7469845438922,20.4292139595574,27.4299129300571));
#54029=CARTESIAN_POINT('Ctrl Pts',(-22.7451303069942,20.4296917756266,27.4300317986192));
#54030=CARTESIAN_POINT('Ctrl Pts',(-22.7407002393559,20.4308375657849,27.430315628073));
#54031=CARTESIAN_POINT('Ctrl Pts',(-22.73812480031,20.4315070801371,27.4304804990021));
#54032=CARTESIAN_POINT('Ctrl Pts',(-22.7294158161583,20.4337825978779,27.4310375726947));
#54033=CARTESIAN_POINT('Ctrl Pts',(-22.7232861316412,20.435403524639,27.4314289114891));
#54034=CARTESIAN_POINT('Ctrl Pts',(-22.7087399555581,20.4392960642139,27.4323558932674));
#54035=CARTESIAN_POINT('Ctrl Pts',(-22.7003277686039,20.4415837716827,27.4328906267321));
#54036=CARTESIAN_POINT('Ctrl Pts',(-22.6019444893796,20.4687684659821,27.4391298196486));
#54037=CARTESIAN_POINT('Ctrl Pts',(-22.5130771912219,20.4975319163713,27.4446218654016));
#54038=CARTESIAN_POINT('Ctrl Pts',(-22.0544632491773,20.6683164457409,27.4728067033159));
#54039=CARTESIAN_POINT('Ctrl Pts',(-21.7120096517425,20.8737155778351,27.49377945799));
#54040=CARTESIAN_POINT('Ctrl Pts',(-21.4013826009653,21.1484154122913,27.5188828837749));
#54041=CARTESIAN_POINT('Ctrl Pts',(-21.3875564295565,21.1608574043582,27.5200138478056));
#54042=CARTESIAN_POINT('Ctrl Pts',(-21.3693915874165,21.1774905403839,27.521518177171));
#54043=CARTESIAN_POINT('Ctrl Pts',(-21.3649556803542,21.1815753488715,27.521887015983));
#54044=CARTESIAN_POINT('Ctrl Pts',(-21.358082892052,21.1879399001831,27.5224607898686));
#54045=CARTESIAN_POINT('Ctrl Pts',(-21.3556380268463,21.1902110335542,27.5226653561409));
#54046=CARTESIAN_POINT('Ctrl Pts',(-21.3507974749491,21.1947216423938,27.5230712836476));
#54047=CARTESIAN_POINT('Ctrl Pts',(-21.3484016700882,21.1969609857506,27.5232726390792));
#54048=CARTESIAN_POINT('Ctrl Pts',(-21.3430790086122,21.2019512870067,27.5237209734844));
#54049=CARTESIAN_POINT('Ctrl Pts',(-21.3401538723117,21.2047040644147,27.5239680307618));
#54050=CARTESIAN_POINT('Ctrl Pts',(-21.3340882117308,21.2104337365192,27.5244817340694));
#54051=CARTESIAN_POINT('Ctrl Pts',(-21.3309485231067,21.2134115006209,27.5247484175147));
#54052=CARTESIAN_POINT('Ctrl Pts',(-21.3228758352996,21.2210987950105,27.5254361314042));
#54053=CARTESIAN_POINT('Ctrl Pts',(-21.3179517900819,21.2258176596019,27.5258575674866));
#54054=CARTESIAN_POINT('Ctrl Pts',(-21.3036771980047,21.2395846339333,27.5270850213888));
#54055=CARTESIAN_POINT('Ctrl Pts',(-21.2943665057809,21.2486737053734,27.5278928297702));
#54056=CARTESIAN_POINT('Ctrl Pts',(-21.2014485395632,21.3404854430537,27.536027696977));
#54057=CARTESIAN_POINT('Ctrl Pts',(-21.1223838088231,21.4276601242072,27.5435539274481));
#54058=CARTESIAN_POINT('Ctrl Pts',(-20.8397993811679,21.7757239019829,27.5729094889668));
#54059=CARTESIAN_POINT('Ctrl Pts',(-20.6721349275666,22.0630063860666,27.5960029633228));
#54060=CARTESIAN_POINT('Ctrl Pts',(-20.5472706802057,22.380497178921,27.6181112965073));
#54061=CARTESIAN_POINT('Ctrl Pts',(-20.5434792949456,22.3902774051277,27.6187889734273));
#54062=CARTESIAN_POINT('Ctrl Pts',(-20.5256350809092,22.4369835498124,27.6220086871245));
#54063=CARTESIAN_POINT('Ctrl Pts',(-20.512213561853,22.4741493203482,27.624521500742));
#54064=CARTESIAN_POINT('Ctrl Pts',(-20.4977673924332,22.5165793663981,27.6273272823384));
#54065=CARTESIAN_POINT('Ctrl Pts',(-20.496068995794,22.5216084396691,27.6276588455048));
#54066=CARTESIAN_POINT('Ctrl Pts',(-20.4936055899177,22.5289626478279,27.6281422257942));
#54067=CARTESIAN_POINT('Ctrl Pts',(-20.4928308033975,22.5312844610493,27.6282946200396));
#54068=CARTESIAN_POINT('Ctrl Pts',(-20.4914637244077,22.5353968022075,27.6285641541264));
#54069=CARTESIAN_POINT('Ctrl Pts',(-20.4908703581276,22.5371869684705,27.6286813580655));
#54070=CARTESIAN_POINT('Ctrl Pts',(-20.4896344374464,22.5409266887467,27.6289259319619));
#54071=CARTESIAN_POINT('Ctrl Pts',(-20.4889921755184,22.5428763319349,27.6290532842275));
#54072=CARTESIAN_POINT('Ctrl Pts',(-20.4873192994737,22.547970869718,27.62938566878));
#54073=CARTESIAN_POINT('Ctrl Pts',(-20.4862916627405,22.5511167507667,27.6295905238155));
#54074=CARTESIAN_POINT('Ctrl Pts',(-20.4818440391499,22.5648035516745,27.6304801036122));
#54075=CARTESIAN_POINT('Ctrl Pts',(-20.4784735350793,22.5753606537141,27.6311619271138));
#54076=CARTESIAN_POINT('Ctrl Pts',(-20.4544231268978,22.6520545818143,27.6360851488371));
#54077=CARTESIAN_POINT('Ctrl Pts',(-20.4358248696428,22.7188313181952,27.6402103518796));
#54078=CARTESIAN_POINT('Ctrl Pts',(-20.3739100262168,22.9725270442527,27.6554594332074));
#54079=CARTESIAN_POINT('Ctrl Pts',(-20.3451543045787,23.1625974644635,27.6660486351879));
#54080=CARTESIAN_POINT('Ctrl Pts',(-20.3191572901728,23.5889542391757,27.6899572850673));
#54081=CARTESIAN_POINT('Ctrl Pts',(-20.3305983639806,23.8246197288227,27.7033167957185));
#54082=CARTESIAN_POINT('Ctrl Pts',(-20.3698698738081,24.0713051023975,27.718476399373));
#54083=CARTESIAN_POINT('Ctrl Pts',(-20.3722567850523,24.0856707378248,27.7193632324363));
#54084=CARTESIAN_POINT('Ctrl Pts',(-20.3756714690803,24.1053943096399,27.7205865136477));
#54085=CARTESIAN_POINT('Ctrl Pts',(-20.3766156303009,24.1107667012417,27.7209202972989));
#54086=CARTESIAN_POINT('Ctrl Pts',(-20.3781391738528,24.1193085823367,27.7214519328993));
#54087=CARTESIAN_POINT('Ctrl Pts',(-20.3787096806937,24.1224796613499,27.7216495015595));
#54088=CARTESIAN_POINT('Ctrl Pts',(-20.3798753041776,24.1289033168727,27.7220501337541));
#54089=CARTESIAN_POINT('Ctrl Pts',(-20.3804706730015,24.1321558433523,27.7222532051284));
#54090=CARTESIAN_POINT('Ctrl Pts',(-20.3818466485864,24.1396080859988,27.7227189856311));
#54091=CARTESIAN_POINT('Ctrl Pts',(-20.3826306004717,24.1438071711841,27.7229818013035));
#54092=CARTESIAN_POINT('Ctrl Pts',(-20.3842908795108,24.1526031595796,27.723533100004));
#54093=CARTESIAN_POINT('Ctrl Pts',(-20.3851688748428,24.1571997343158,27.7238216358814));
#54094=CARTESIAN_POINT('Ctrl Pts',(-20.3875103833517,24.1693149988796,27.7245833035799));
#54095=CARTESIAN_POINT('Ctrl Pts',(-20.3889906893279,24.1768303780561,27.7250569721817));
#54096=CARTESIAN_POINT('Ctrl Pts',(-20.3934976711492,24.1992893446802,27.7264760765324));
#54097=CARTESIAN_POINT('Ctrl Pts',(-20.3966035849002,24.2142166434354,27.7274240453669));
#54098=CARTESIAN_POINT('Ctrl Pts',(-20.4079331102722,24.2667937676483,27.7307801134687));
#54099=CARTESIAN_POINT('Ctrl Pts',(-20.4167257314593,24.3043163710793,27.7332063342722));
#54100=CARTESIAN_POINT('Ctrl Pts',(-20.4623139241014,24.4842722630159,27.7449967493157));
#54101=CARTESIAN_POINT('Ctrl Pts',(-20.5081554938185,24.6242140151136,27.7546463011361));
#54102=CARTESIAN_POINT('Ctrl Pts',(-20.6741517893392,25.033882329867,27.7842219637196));
#54103=CARTESIAN_POINT('Ctrl Pts',(-20.8219167530609,25.2907425579738,27.8047015212794));
#54104=CARTESIAN_POINT('Ctrl Pts',(-21.0121190377125,25.5362635201789,27.8243465830336));
#54105=CARTESIAN_POINT('Ctrl Pts',(-21.021769544954,25.548535566931,27.8253283232041));
#54106=CARTESIAN_POINT('Ctrl Pts',(-21.0337159365839,25.5635020547531,27.8265248689699));
#54107=CARTESIAN_POINT('Ctrl Pts',(-21.035927358597,25.5662631965599,27.8267455862883));
#54108=CARTESIAN_POINT('Ctrl Pts',(-21.0395903844625,25.5708213826238,27.8271098939513));
#54109=CARTESIAN_POINT('Ctrl Pts',(-21.0410393742911,25.572620507527,27.827253671413));
#54110=CARTESIAN_POINT('Ctrl Pts',(-21.0435451037207,25.5757248848473,27.8275017293103));
#54111=CARTESIAN_POINT('Ctrl Pts',(-21.0446009272821,25.5770308669344,27.8276060759109));
#54112=CARTESIAN_POINT('Ctrl Pts',(-21.0469750606858,25.579962818239,27.82784031506));
#54113=CARTESIAN_POINT('Ctrl Pts',(-21.0482939317837,25.581588325835,27.827970165904));
#54114=CARTESIAN_POINT('Ctrl Pts',(-21.0518161929987,25.5859208757361,27.8283162301519));
#54115=CARTESIAN_POINT('Ctrl Pts',(-21.0540224066314,25.5886256350419,27.8285322385175));
#54116=CARTESIAN_POINT('Ctrl Pts',(-21.0643698071359,25.6012692800458,27.8295418520452));
#54117=CARTESIAN_POINT('Ctrl Pts',(-21.0725661340474,25.6111631921255,27.8303314972888));
#54118=CARTESIAN_POINT('Ctrl Pts',(-21.2701981508566,25.8468446253154,27.8491392604071));
#54119=CARTESIAN_POINT('Ctrl Pts',(-21.4896959486678,26.0456798741573,27.8650455520782));
#54120=CARTESIAN_POINT('Ctrl Pts',(-21.8429133622767,26.2868114479692,27.8891137015016));
#54121=CARTESIAN_POINT('Ctrl Pts',(-21.9570772617629,26.3548047014022,27.8966842956439));
#54122=CARTESIAN_POINT('Ctrl Pts',(-22.0750363456406,26.4155369446113,27.9044917472066));
#54123=CARTESIAN_POINT('Origin',(-23.5502525316942,23.5502525316942,-77.3107734492734));
#54124=CARTESIAN_POINT('',(-22.0750360153459,26.4155367745562,29.4036987823186));
#54125=CARTESIAN_POINT('',(-22.0750360153802,26.4155367745738,29.1557101328919));
#54126=CARTESIAN_POINT('',(-22.0750360153461,26.4155367745563,-77.3107734492734));
#54127=CARTESIAN_POINT('',(-26.7730011212944,23.5472374479352,28.5607734493046));
#54128=CARTESIAN_POINT('Ctrl Pts',(-26.7730011212944,23.5472374479352,28.5607734493046));
#54129=CARTESIAN_POINT('Ctrl Pts',(-26.7728770430253,23.4146132495376,28.5689619155671));
#54130=CARTESIAN_POINT('Ctrl Pts',(-26.7645626120231,23.2823550477187,28.5771503818296));
#54131=CARTESIAN_POINT('Ctrl Pts',(-26.7482144162662,23.1513072380455,28.5853388480921));
#54132=CARTESIAN_POINT('Ctrl Pts',(-26.733272166814,23.0315295517846,28.59282310552));
#54133=CARTESIAN_POINT('Ctrl Pts',(-26.7116191815025,22.9127623390399,28.6003073629479));
#54134=CARTESIAN_POINT('Ctrl Pts',(-26.6834084421646,22.7956323602277,28.6077916203757));
#54135=CARTESIAN_POINT('Ctrl Pts',(-26.6601379603629,22.6990141536737,28.6139652365362));
#54136=CARTESIAN_POINT('Ctrl Pts',(-26.6323532111562,22.6033035052964,28.6201388526966));
#54137=CARTESIAN_POINT('Ctrl Pts',(-26.6001402414619,22.5089540536834,28.6263124688571));
#54138=CARTESIAN_POINT('Ctrl Pts',(-26.5679709395546,22.4147325018507,28.6324777160854));
#54139=CARTESIAN_POINT('Ctrl Pts',(-26.5313854877104,22.3218688864176,28.6386429633138));
#54140=CARTESIAN_POINT('Ctrl Pts',(-26.4905206292591,22.2308052697916,28.6448082105422));
#54141=CARTESIAN_POINT('Ctrl Pts',(-26.4496991068733,22.1398382236423,28.6509669196944));
#54142=CARTESIAN_POINT('Ctrl Pts',(-26.4046073770992,22.0506677752294,28.6571256288465));
#54143=CARTESIAN_POINT('Ctrl Pts',(-26.3554312203936,21.9637185462508,28.6632843379987));
#54144=CARTESIAN_POINT('Ctrl Pts',(-26.3062911453097,21.8768331138232,28.6694385283713));
#54145=CARTESIAN_POINT('Ctrl Pts',(-26.2530728147334,21.7921660373047,28.6755927187439));
#54146=CARTESIAN_POINT('Ctrl Pts',(-26.196008722109,21.710118910627,28.6817469091165));
#54147=CARTESIAN_POINT('Ctrl Pts',(-26.1389663707552,21.6281030436909,28.6878987547585));
#54148=CARTESIAN_POINT('Ctrl Pts',(-26.0780814164171,21.5487054992064,28.6940506004006));
#54149=CARTESIAN_POINT('Ctrl Pts',(-26.0136301234778,21.4722995960389,28.7002024460427));
#54150=CARTESIAN_POINT('Ctrl Pts',(-25.9491861651483,21.3959023879257,28.7063535915997));
#54151=CARTESIAN_POINT('Ctrl Pts',(-25.8811769550647,21.3224964761269,28.7125047371567));
#54152=CARTESIAN_POINT('Ctrl Pts',(-25.8099189146665,21.2524219460842,28.7186558827137));
#54153=CARTESIAN_POINT('Ctrl Pts',(-25.7386499437626,21.1823366670784,28.7248079718152));
#54154=CARTESIAN_POINT('Ctrl Pts',(-25.6641314623008,21.1155840892799,28.7309600609167));
#54155=CARTESIAN_POINT('Ctrl Pts',(-25.5867158622222,21.0524665789123,28.7371121500182));
#54156=CARTESIAN_POINT('Ctrl Pts',(-25.509217864773,20.9892818893599,28.7432707871018));
#54157=CARTESIAN_POINT('Ctrl Pts',(-25.4288169282932,20.9297402681568,28.7494294241854));
#54158=CARTESIAN_POINT('Ctrl Pts',(-25.3458974682944,20.8741029050549,28.755588061269));
#54159=CARTESIAN_POINT('Ctrl Pts',(-25.2629319668925,20.8184346490568,28.7617501179636));
#54160=CARTESIAN_POINT('Ctrl Pts',(-25.1774455283915,20.7666751934139,28.7679121746582));
#54161=CARTESIAN_POINT('Ctrl Pts',(-25.0898486030466,20.7190405121562,28.7740742313527));
#54162=CARTESIAN_POINT('Ctrl Pts',(-25.0021056968023,20.6713264473633,28.7802465571586));
#54163=CARTESIAN_POINT('Ctrl Pts',(-24.9122456691325,20.6277510771515,28.7864188829645));
#54164=CARTESIAN_POINT('Ctrl Pts',(-24.8207005657972,20.5884828993386,28.7925912087704));
#54165=CARTESIAN_POINT('Ctrl Pts',(-24.7510549962827,20.5586085040085,28.7972869830972));
#54166=CARTESIAN_POINT('Ctrl Pts',(-24.6804345781804,20.5312260596704,28.801982757424));
#54167=CARTESIAN_POINT('Ctrl Pts',(-24.6090348746265,20.5063902626691,28.8066785317507));
#54168=CARTESIAN_POINT('Ctrl Pts',(-24.5151585414876,20.4737361557608,28.8128525360266));
#54169=CARTESIAN_POINT('Ctrl Pts',(-24.4196057560507,20.4453718170294,28.8190265403026));
#54170=CARTESIAN_POINT('Ctrl Pts',(-24.3228048326036,20.4214699401964,28.8252005445785));
#54171=CARTESIAN_POINT('Ctrl Pts',(-24.2261346830957,20.3976003537846,28.8313662080367));
#54172=CARTESIAN_POINT('Ctrl Pts',(-24.12822016485,20.3781813497186,28.8375318714949));
#54173=CARTESIAN_POINT('Ctrl Pts',(-24.0295072351286,20.3633367041682,28.8436975349531));
#54174=CARTESIAN_POINT('Ctrl Pts',(-23.9308985456846,20.3485077344767,28.8498566875067));
#54175=CARTESIAN_POINT('Ctrl Pts',(-23.8314935478987,20.33824358386,28.8560158400603));
#54176=CARTESIAN_POINT('Ctrl Pts',(-23.7317500115561,20.3326173399262,28.8621749926138));
#54177=CARTESIAN_POINT('Ctrl Pts',(-23.6320790295015,20.3269951885697,28.868329664948));
#54178=CARTESIAN_POINT('Ctrl Pts',(-23.5320704305932,20.3260042607985,28.8744843372822));
#54179=CARTESIAN_POINT('Ctrl Pts',(-23.4321878439339,20.3296658938277,28.8806390096164));
#54180=CARTESIAN_POINT('Ctrl Pts',(-23.3323429288885,20.3333261458392,28.8867913606606));
#54181=CARTESIAN_POINT('Ctrl Pts',(-23.2326243649712,20.3416354560159,28.8929437117048));
#54182=CARTESIAN_POINT('Ctrl Pts',(-23.1334956335591,20.3545630520425,28.8990960627491));
#54183=CARTESIAN_POINT('Ctrl Pts',(-23.0343778166042,20.3674892246907,28.9052477363957));
#54184=CARTESIAN_POINT('Ctrl Pts',(-22.9358501334765,20.3850326160794,28.9113994100423));
#54185=CARTESIAN_POINT('Ctrl Pts',(-22.8383697942054,20.4071107069326,28.9175510836889));
#54186=CARTESIAN_POINT('Ctrl Pts',(-22.7408741555218,20.4291922629135,28.9237037228327));
#54187=CARTESIAN_POINT('Ctrl Pts',(-22.644426610603,20.4558098361482,28.9298563619764));
#54188=CARTESIAN_POINT('Ctrl Pts',(-22.5494720627858,20.486830259863,28.9360090011202));
#54189=CARTESIAN_POINT('Ctrl Pts',(-22.4544159917333,20.5178838499068,28.9421682185253));
#54190=CARTESIAN_POINT('Ctrl Pts',(-22.3608565188245,20.5533495556489,28.9483274359304));
#54191=CARTESIAN_POINT('Ctrl Pts',(-22.2692212022268,20.5930450152316,28.9544866533355));
#54192=CARTESIAN_POINT('Ctrl Pts',(-22.1775347462838,20.6327626278431,28.9606493080436));
#54193=CARTESIAN_POINT('Ctrl Pts',(-22.0877749750697,20.6767145044222,28.9668119627517));
#54194=CARTESIAN_POINT('Ctrl Pts',(-22.0003454654848,20.724671945582,28.9729746174598));
#54195=CARTESIAN_POINT('Ctrl Pts',(-21.9127699496478,20.7727094751042,28.9791475637287));
#54196=CARTESIAN_POINT('Ctrl Pts',(-21.827532839302,20.8247657045023,28.9853205099976));
#54197=CARTESIAN_POINT('Ctrl Pts',(-21.7450094316521,20.8805681098476,28.9914934562665));
#54198=CARTESIAN_POINT('Ctrl Pts',(-21.6823020275795,20.9229709150621,28.9961841185529));
#54199=CARTESIAN_POINT('Ctrl Pts',(-21.6211609510266,20.9675358869179,29.0008747808392));
#54200=CARTESIAN_POINT('Ctrl Pts',(-21.5617373904308,21.0141285017094,29.0055654431255));
#54201=CARTESIAN_POINT('Ctrl Pts',(-21.4836644003982,21.0753436950391,29.0117282180629));
#54202=CARTESIAN_POINT('Ctrl Pts',(-21.4082807768226,21.1402771855626,29.0178909930002));
#54203=CARTESIAN_POINT('Ctrl Pts',(-21.3359627690922,21.2086636673254,29.0240537679376));
#54204=CARTESIAN_POINT('Ctrl Pts',(-21.2637431363746,21.2769571221751,29.0302081595817));
#54205=CARTESIAN_POINT('Ctrl Pts',(-21.1945811452636,21.3486939361772,29.0363625512258));
#54206=CARTESIAN_POINT('Ctrl Pts',(-21.1288215339032,21.4235674385417,29.0425169428699));
#54207=CARTESIAN_POINT('Ctrl Pts',(-21.0631317896435,21.498361390641,29.0486647957057));
#54208=CARTESIAN_POINT('Ctrl Pts',(-21.0008375249201,21.5762850804529,29.0548126485414));
#54209=CARTESIAN_POINT('Ctrl Pts',(-20.9422472978569,21.6569944238872,29.0609605013771));
#54210=CARTESIAN_POINT('Ctrl Pts',(-20.8836997349241,21.737644996531,29.06710387748));
#54211=CARTESIAN_POINT('Ctrl Pts',(-20.8288511029882,21.8210768387006,29.0732472535828));
#54212=CARTESIAN_POINT('Ctrl Pts',(-20.777969646471,21.9069128933971,29.0793906296856));
#54213=CARTESIAN_POINT('Ctrl Pts',(-20.7271073720606,21.9927165882423,29.0855316897601));
#54214=CARTESIAN_POINT('Ctrl Pts',(-20.6802095235959,22.0809223203237,29.0916727498346));
#54215=CARTESIAN_POINT('Ctrl Pts',(-20.6375004593718,22.1711249351021,29.097813809909));
#54216=CARTESIAN_POINT('Ctrl Pts',(-20.5947959805517,22.2613178653924,29.1039542106565));
#54217=CARTESIAN_POINT('Ctrl Pts',(-20.5562795784705,22.35350685826,29.1100946114039));
#54218=CARTESIAN_POINT('Ctrl Pts',(-20.5221287030737,22.4472640272027,29.1162350121513));
#54219=CARTESIAN_POINT('Ctrl Pts',(-20.4879722860564,22.5410364100055,29.122376409294));
#54220=CARTESIAN_POINT('Ctrl Pts',(-20.4581829518959,22.6363770647411,29.1285178064367));
#54221=CARTESIAN_POINT('Ctrl Pts',(-20.4328888926931,22.7328410657029,29.1346592035794));
#54222=CARTESIAN_POINT('Ctrl Pts',(-20.4075672588473,22.8294102281326,29.1408072958449));
#54223=CARTESIAN_POINT('Ctrl Pts',(-20.3867507965031,22.9271047597847,29.1469553881104));
#54224=CARTESIAN_POINT('Ctrl Pts',(-20.3705169339306,23.0254677274028,29.153103480376));
#54225=CARTESIAN_POINT('Ctrl Pts',(-20.3542738710606,23.1238864407539,29.1592550569804));
#54226=CARTESIAN_POINT('Ctrl Pts',(-20.3426186303105,23.2229739115664,29.1654066335848));
#54227=CARTESIAN_POINT('Ctrl Pts',(-20.335576687458,23.322268367805,29.1715582101892));
#54228=CARTESIAN_POINT('Ctrl Pts',(-20.3285227426266,23.4217320571646,29.1777202712713));
#54229=CARTESIAN_POINT('Ctrl Pts',(-20.3260978114541,23.5214030007143,29.1838823323533));
#54230=CARTESIAN_POINT('Ctrl Pts',(-20.3282752106598,23.6208195582726,29.1900443934354));
#54231=CARTESIAN_POINT('Ctrl Pts',(-20.3299722555587,23.6983039081485,29.1948470471237));
#54232=CARTESIAN_POINT('Ctrl Pts',(-20.3344639246531,23.7756337186087,29.1996497008121));
#54233=CARTESIAN_POINT('Ctrl Pts',(-20.3417159218685,23.8525940371284,29.2044523545004));
#54234=CARTESIAN_POINT('Ctrl Pts',(-20.3510543363531,23.9516960268091,29.2106367433571));
#54235=CARTESIAN_POINT('Ctrl Pts',(-20.3650046499201,24.0505365678241,29.2168211322138));
#54236=CARTESIAN_POINT('Ctrl Pts',(-20.3835453683844,24.1486531536376,29.2230055210705));
#54237=CARTESIAN_POINT('Ctrl Pts',(-20.4020609124087,24.2466365175319,29.2291815128132));
#54238=CARTESIAN_POINT('Ctrl Pts',(-20.4251543921595,24.343897458819,29.2353575045559));
#54239=CARTESIAN_POINT('Ctrl Pts',(-20.4527524934316,24.4399778125889,29.2415334962986));
#54240=CARTESIAN_POINT('Ctrl Pts',(-20.4803211919858,24.5359558033916,29.2477029082067));
#54241=CARTESIAN_POINT('Ctrl Pts',(-20.5123848512336,24.6307552940067,29.2538723201149));
#54242=CARTESIAN_POINT('Ctrl Pts',(-20.5488191522555,24.7239284798551,29.260041732023));
#54243=CARTESIAN_POINT('Ctrl Pts',(-20.5852261414904,24.8170318214594,29.2662065192324));
#54244=CARTESIAN_POINT('Ctrl Pts',(-20.625997100487,24.9085108808592,29.2723713064417));
#54245=CARTESIAN_POINT('Ctrl Pts',(-20.6709582176269,24.9979340627913,29.2785360936511));
#54246=CARTESIAN_POINT('Ctrl Pts',(-20.7159017341586,25.0873222388674,29.2846984675752));
#54247=CARTESIAN_POINT('Ctrl Pts',(-20.7650319550941,25.1746557508006,29.2908608414993));
#54248=CARTESIAN_POINT('Ctrl Pts',(-20.8181277354351,25.2595247920922,29.2970232154234));
#54249=CARTESIAN_POINT('Ctrl Pts',(-20.8712167881162,25.3443830797978,29.3031848085254));
#54250=CARTESIAN_POINT('Ctrl Pts',(-20.9282701716987,25.4267771510795,29.3093464016274));
#54251=CARTESIAN_POINT('Ctrl Pts',(-20.9890222710729,25.506324389929,29.3155079947294));
#54252=CARTESIAN_POINT('Ctrl Pts',(-21.0497827567766,25.5858826096227,29.3216704383889));
#54253=CARTESIAN_POINT('Ctrl Pts',(-21.1142427097965,25.6625928725552,29.3278328820483));
#54254=CARTESIAN_POINT('Ctrl Pts',(-21.1820955375943,25.7361047713928,29.3339953257078));
#54255=CARTESIAN_POINT('Ctrl Pts',(-21.2500181805297,25.8096923081,29.3401641100293));
#54256=CARTESIAN_POINT('Ctrl Pts',(-21.3213403757397,25.8800745904679,29.3463328943509));
#54257=CARTESIAN_POINT('Ctrl Pts',(-21.395717967883,25.9469374037295,29.3525016786724));
#54258=CARTESIAN_POINT('Ctrl Pts',(-21.4701355884634,26.0138362011342,29.3586737829024));
#54259=CARTESIAN_POINT('Ctrl Pts',(-21.5476115464694,26.0772114826441,29.3648458871323));
#54260=CARTESIAN_POINT('Ctrl Pts',(-21.6277694384365,26.1367900471071,29.3710179913623));
#54261=CARTESIAN_POINT('Ctrl Pts',(-21.7080572364831,26.1964651662266,29.3772000982737));
#54262=CARTESIAN_POINT('Ctrl Pts',(-21.7910352916877,26.2523310354384,29.3833822051852));
#54263=CARTESIAN_POINT('Ctrl Pts',(-21.8762990308253,26.3041583469734,29.3895643120967));
#54264=CARTESIAN_POINT('Ctrl Pts',(-21.9396271745814,26.3426521717644,29.3941559633562));
#54265=CARTESIAN_POINT('Ctrl Pts',(-22.0042156407435,26.3789190481311,29.3987476146158));
#54266=CARTESIAN_POINT('Ctrl Pts',(-22.0698912045492,26.4128820752422,29.4033392658753));
#54267=CARTESIAN_POINT('Ctrl Pts',(-22.0716052898007,26.4137684859632,29.4034591046898));
#54268=CARTESIAN_POINT('Ctrl Pts',(-22.0733202276715,26.4146533863471,29.4035789435042));
#54269=CARTESIAN_POINT('Ctrl Pts',(-22.0750360153459,26.4155367745562,29.4036987823186));
#54270=CARTESIAN_POINT('Ctrl Pts',(-26.7730011251471,23.5472415688628,28.5608472020237));
#54271=CARTESIAN_POINT('Ctrl Pts',(-26.7732052327801,23.7657057692041,28.5486405204165));
#54272=CARTESIAN_POINT('Ctrl Pts',(-26.7511964717817,23.9836060593955,28.5363786813096));
#54273=CARTESIAN_POINT('Ctrl Pts',(-26.6975842485767,24.2450678492038,28.5204949993101));
#54274=CARTESIAN_POINT('Ctrl Pts',(-26.6867827696282,24.2923057258727,28.517579823793));
#54275=CARTESIAN_POINT('Ctrl Pts',(-26.6732345673099,24.3459586406051,28.5142107461922));
#54276=CARTESIAN_POINT('Ctrl Pts',(-26.6715267876305,24.3526315098634,28.5137907009532));
#54277=CARTESIAN_POINT('Ctrl Pts',(-26.6687045815779,24.3635134572781,28.5131040008554));
#54278=CARTESIAN_POINT('Ctrl Pts',(-26.6676029880457,24.3677258661197,28.5128377620448));
#54279=CARTESIAN_POINT('Ctrl Pts',(-26.6654495553398,24.3758927746728,28.5123207708302));
#54280=CARTESIAN_POINT('Ctrl Pts',(-26.6643987139196,24.379847530739,28.5120700512362));
#54281=CARTESIAN_POINT('Ctrl Pts',(-26.662559223334,24.3867175581329,28.5116338632029));
#54282=CARTESIAN_POINT('Ctrl Pts',(-26.6617740012806,24.3896337487135,28.5114485065059));
#54283=CARTESIAN_POINT('Ctrl Pts',(-26.6601297659965,24.3957061671889,28.5110621101178));
#54284=CARTESIAN_POINT('Ctrl Pts',(-26.6592700446441,24.398862198296,28.5108610475363));
#54285=CARTESIAN_POINT('Ctrl Pts',(-26.656895218863,24.4075281182112,28.5103083018023));
#54286=CARTESIAN_POINT('Ctrl Pts',(-26.6553702676289,24.4130352750817,28.5099562978897));
#54287=CARTESIAN_POINT('Ctrl Pts',(-26.6494321890629,24.4342601887979,28.5085967908123));
#54288=CARTESIAN_POINT('Ctrl Pts',(-26.6449143593179,24.4499481709622,28.5075858730496));
#54289=CARTESIAN_POINT('Ctrl Pts',(-26.5682243849988,24.7088375135347,28.4908009274684));
#54290=CARTESIAN_POINT('Ctrl Pts',(-26.4677199651157,24.9426619677442,28.4740341061042));
#54291=CARTESIAN_POINT('Ctrl Pts',(-26.3181482739264,25.2015963512007,28.4538243368009));
#54292=CARTESIAN_POINT('Ctrl Pts',(-26.2945847993518,25.2404666075435,28.4507462420151));
#54293=CARTESIAN_POINT('Ctrl Pts',(-26.2468732310488,25.3155420147868,28.4447248746834));
#54294=CARTESIAN_POINT('Ctrl Pts',(-26.2227979264607,25.3517828079685,28.441782062865));
#54295=CARTESIAN_POINT('Ctrl Pts',(-26.1340127413415,25.4797335394188,28.4312832000252));
#54296=CARTESIAN_POINT('Ctrl Pts',(-26.0652505777227,25.5685445966407,28.4237880085619));
#54297=CARTESIAN_POINT('Ctrl Pts',(-25.9617489097634,25.6886981409627,28.4135279749305));
#54298=CARTESIAN_POINT('Ctrl Pts',(-25.9307532497951,25.7231495138557,28.4105714585326));
#54299=CARTESIAN_POINT('Ctrl Pts',(-25.8962741622837,25.7598489186474,28.4074172765493));
#54300=CARTESIAN_POINT('Ctrl Pts',(-25.8935193960734,25.7627701219398,28.4071661765245));
#54301=CARTESIAN_POINT('Ctrl Pts',(-25.8890424176267,25.7674998495487,28.4067595775438));
#54302=CARTESIAN_POINT('Ctrl Pts',(-25.8873235607179,25.7693115224541,28.4066038239335));
#54303=CARTESIAN_POINT('Ctrl Pts',(-25.8839997423051,25.7728066771356,28.4063033213533));
#54304=CARTESIAN_POINT('Ctrl Pts',(-25.8823950615293,25.7744904220894,28.4061585508721));
#54305=CARTESIAN_POINT('Ctrl Pts',(-25.8794997381004,25.7775218229659,28.4058978965794));
#54306=CARTESIAN_POINT('Ctrl Pts',(-25.8782097531349,25.7788700896399,28.4057819625563));
#54307=CARTESIAN_POINT('Ctrl Pts',(-25.8754343976114,25.7817657971123,28.4055329601953));
#54308=CARTESIAN_POINT('Ctrl Pts',(-25.8739486573939,25.7833128709595,28.4053999219466));
#54309=CARTESIAN_POINT('Ctrl Pts',(-25.8699464878757,25.7874719368959,28.4050422518339));
#54310=CARTESIAN_POINT('Ctrl Pts',(-25.8674271824342,25.7900811759505,28.4048178445526));
#54311=CARTESIAN_POINT('Ctrl Pts',(-25.855854113568,25.8020269540329,28.4037903318898));
#54312=CARTESIAN_POINT('Ctrl Pts',(-25.8467481239361,25.8113130598078,28.4029912601999));
#54313=CARTESIAN_POINT('Ctrl Pts',(-25.6830586238193,25.9762313004227,28.3887884107199));
#54314=CARTESIAN_POINT('Ctrl Pts',(-25.5130117965697,26.1157629175801,28.3765642749067));
#54315=CARTESIAN_POINT('Ctrl Pts',(-25.2325058369869,26.3015867985429,28.3577627383615));
#54316=CARTESIAN_POINT('Ctrl Pts',(-25.1314851885689,26.3608607272297,28.351230950272));
#54317=CARTESIAN_POINT('Ctrl Pts',(-24.9240760554497,26.467830237088,28.337956983082));
#54318=CARTESIAN_POINT('Ctrl Pts',(-24.8178824683506,26.5155115583233,28.3312259744154));
#54319=CARTESIAN_POINT('Ctrl Pts',(-24.6780767387035,26.5694003436548,28.3223058079386));
#54320=CARTESIAN_POINT('Ctrl Pts',(-24.6466173586655,26.5809661427991,28.3202952161408));
#54321=CARTESIAN_POINT('Ctrl Pts',(-24.5953835567667,26.5988997659439,28.3170125701837));
#54322=CARTESIAN_POINT('Ctrl Pts',(-24.5757174545188,26.6055709241279,28.3157505872963));
#54323=CARTESIAN_POINT('Ctrl Pts',(-24.5517423539163,26.6134462367334,28.3142093292167));
#54324=CARTESIAN_POINT('Ctrl Pts',(-24.5474932248197,26.6148321991631,28.3139360657904));
#54325=CARTESIAN_POINT('Ctrl Pts',(-24.5392675926891,26.6174962810254,28.3134068630366));
#54326=CARTESIAN_POINT('Ctrl Pts',(-24.5352914589502,26.6187755184446,28.3131509611152));
#54327=CARTESIAN_POINT('Ctrl Pts',(-24.5284223217407,26.6209707917981,28.3127087004477));
#54328=CARTESIAN_POINT('Ctrl Pts',(-24.5255304837352,26.6218904802903,28.3125224622548));
#54329=CARTESIAN_POINT('Ctrl Pts',(-24.5195473490813,26.623783989798,28.3121370334584));
#54330=CARTESIAN_POINT('Ctrl Pts',(-24.5164558746813,26.6247572343818,28.3119378241248));
#54331=CARTESIAN_POINT('Ctrl Pts',(-24.5080699203258,26.6273833667659,28.311397284801));
#54332=CARTESIAN_POINT('Ctrl Pts',(-24.5027726508505,26.6290272470804,28.3110556592819));
#54333=CARTESIAN_POINT('Ctrl Pts',(-24.4829904286147,26.6351102428535,28.3097792126744));
#54334=CARTESIAN_POINT('Ctrl Pts',(-24.46847865157,26.6394608222807,28.3088414936667));
#54335=CARTESIAN_POINT('Ctrl Pts',(-24.2209512445699,26.7117704440484,28.2928223847464));
#54336=CARTESIAN_POINT('Ctrl Pts',(-23.9810734928331,26.7532790394524,28.2768391948932));
#54337=CARTESIAN_POINT('Ctrl Pts',(-23.581482004816,26.7767050619091,28.2498291584829));
#54338=CARTESIAN_POINT('Ctrl Pts',(-23.4236347819836,26.7743711998989,28.2390866274553));
#54339=CARTESIAN_POINT('Ctrl Pts',(-23.1711705404608,26.7520630098291,28.2222540672274));
#54340=CARTESIAN_POINT('Ctrl Pts',(-23.0761636222282,26.7393805031465,28.2160038763618));
#54341=CARTESIAN_POINT('Ctrl Pts',(-22.9716579381135,26.7206552105916,28.2093216273621));
#54342=CARTESIAN_POINT('Ctrl Pts',(-22.9614710397305,26.7187791943223,28.2086723231425));
#54343=CARTESIAN_POINT('Ctrl Pts',(-22.9489223992816,26.7164056322464,28.2078751765298));
#54344=CARTESIAN_POINT('Ctrl Pts',(-22.946552094915,26.7159545339374,28.207724722662));
#54345=CARTESIAN_POINT('Ctrl Pts',(-22.9419564599334,26.7150745784358,28.2074332501457));
#54346=CARTESIAN_POINT('Ctrl Pts',(-22.9397310716364,26.71464603525,28.207292213675));
#54347=CARTESIAN_POINT('Ctrl Pts',(-22.9356928001506,26.713863966487,28.207036478556));
#54348=CARTESIAN_POINT('Ctrl Pts',(-22.9338797745739,26.7135112309343,28.206921734999));
#54349=CARTESIAN_POINT('Ctrl Pts',(-22.9302015623798,26.7127923292127,28.2066890919444));
#54350=CARTESIAN_POINT('Ctrl Pts',(-22.9283364036013,26.7124260729631,28.2065711981951));
#54351=CARTESIAN_POINT('Ctrl Pts',(-22.922967651316,26.7113668916332,28.2062320626084));
#54352=CARTESIAN_POINT('Ctrl Pts',(-22.919464870047,26.7106697895845,28.2060110608988));
#54353=CARTESIAN_POINT('Ctrl Pts',(-22.9040839224942,26.7075821780507,28.205041756317));
#54354=CARTESIAN_POINT('Ctrl Pts',(-22.8922179307233,26.7051304757975,28.2042969221138));
#54355=CARTESIAN_POINT('Ctrl Pts',(-22.6882694481591,26.6617907538697,28.1915415353527));
#54356=CARTESIAN_POINT('Ctrl Pts',(-22.500273182098,26.6034890787997,28.1804827253851));
#54357=CARTESIAN_POINT('Ctrl Pts',(-22.2359402074733,26.4941831285167,28.1644763297204));
#54358=CARTESIAN_POINT('Ctrl Pts',(-22.1546382446509,26.4565206784539,28.1594877959985));
#54359=CARTESIAN_POINT('Ctrl Pts',(-22.0750359096863,26.4155367201564,28.1544576001758));
#54360=CARTESIAN_POINT('',(-26.7730024951077,23.5507381430868,28.3112187782627));
#54361=CARTESIAN_POINT('Ctrl Pts',(-22.0750363456406,26.4155369446113,27.9044917472066));
#54362=CARTESIAN_POINT('Ctrl Pts',(-22.1370108204797,26.4474450330344,27.9085937009903));
#54363=CARTESIAN_POINT('Ctrl Pts',(-22.2000329815414,26.477348858093,27.9127595589773));
#54364=CARTESIAN_POINT('Ctrl Pts',(-22.2754514881685,26.510177471065,27.9177582064902));
#54365=CARTESIAN_POINT('Ctrl Pts',(-22.2869243926363,26.5150923846166,27.9185189556714));
#54366=CARTESIAN_POINT('Ctrl Pts',(-22.3026654277518,26.5217277802182,27.9195632770429));
#54367=CARTESIAN_POINT('Ctrl Pts',(-22.3069092276057,26.5235059958872,27.9198448825534));
#54368=CARTESIAN_POINT('Ctrl Pts',(-22.3141470301014,26.5265205377674,27.920325260705));
#54369=CARTESIAN_POINT('Ctrl Pts',(-22.3171391241759,26.5277614534486,27.9205238771448));
#54370=CARTESIAN_POINT('Ctrl Pts',(-22.3231860273209,26.5302586166514,27.9209253338485));
#54371=CARTESIAN_POINT('Ctrl Pts',(-22.3262409061166,26.5315146826734,27.9211281799381));
#54372=CARTESIAN_POINT('Ctrl Pts',(-22.33320981648,26.5343675531553,27.9215909942883));
#54373=CARTESIAN_POINT('Ctrl Pts',(-22.3371250635236,26.5359613550164,27.9218510639175));
#54374=CARTESIAN_POINT('Ctrl Pts',(-22.3453239613838,26.5392801374906,27.9223957899415));
#54375=CARTESIAN_POINT('Ctrl Pts',(-22.3496082038766,26.5410036222208,27.9226804963259));
#54376=CARTESIAN_POINT('Ctrl Pts',(-22.3608714063266,26.5455065329968,27.9234291650558));
#54377=CARTESIAN_POINT('Ctrl Pts',(-22.3678563755703,26.548270764152,27.9238936398385));
#54378=CARTESIAN_POINT('Ctrl Pts',(-22.388676247457,26.5564259407559,27.925278658544));
#54379=CARTESIAN_POINT('Ctrl Pts',(-22.4025386661893,26.561745666416,27.9262015934575));
#54380=CARTESIAN_POINT('Ctrl Pts',(-22.4512479136405,26.580052752147,27.9294474670952));
#54381=CARTESIAN_POINT('Ctrl Pts',(-22.4862812751604,26.5925321876661,27.9317872303062));
#54382=CARTESIAN_POINT('Ctrl Pts',(-22.6514537013537,26.6481673081038,27.942846478607));
#54383=CARTESIAN_POINT('Ctrl Pts',(-22.7840299422326,26.6835910023773,27.9518124347171));
#54384=CARTESIAN_POINT('Ctrl Pts',(-23.17559622144,26.7618752160113,27.9784517532854));
#54385=CARTESIAN_POINT('Ctrl Pts',(-23.4380487111231,26.7817064112265,27.9965756940932));
#54386=CARTESIAN_POINT('Ctrl Pts',(-23.7007834385039,26.7694851460926,28.0136968013963));
#54387=CARTESIAN_POINT('Ctrl Pts',(-23.7015680801068,26.7694483605199,28.0137479225244));
#54388=CARTESIAN_POINT('Ctrl Pts',(-23.705411549764,26.7692667626366,28.0139982836235));
#54389=CARTESIAN_POINT('Ctrl Pts',(-23.7084701935041,26.7691178770476,28.0141973683649));
#54390=CARTESIAN_POINT('Ctrl Pts',(-23.7185649763606,26.7686120700184,28.0148539142029));
#54391=CARTESIAN_POINT('Ctrl Pts',(-23.7256002064051,26.7682364333955,28.0153106453887));
#54392=CARTESIAN_POINT('Ctrl Pts',(-23.7399359132502,26.7674238456701,28.0162395686254));
#54393=CARTESIAN_POINT('Ctrl Pts',(-23.7472362567654,26.7669851072643,28.0167116850798));
#54394=CARTESIAN_POINT('Ctrl Pts',(-23.7942434687685,26.7639994258681,28.0197454083601));
#54395=CARTESIAN_POINT('Ctrl Pts',(-23.8339040276543,26.76074203758,28.0222762763525));
#54396=CARTESIAN_POINT('Ctrl Pts',(-23.8787882269132,26.756217308299,28.0251002356253));
#54397=CARTESIAN_POINT('Ctrl Pts',(-23.8840788964053,26.7556707276637,28.0254324705672));
#54398=CARTESIAN_POINT('Ctrl Pts',(-23.8918043452103,26.7548532747308,28.0259166479695));
#54399=CARTESIAN_POINT('Ctrl Pts',(-23.8942401720074,26.754592723839,28.0260691702243));
#54400=CARTESIAN_POINT('Ctrl Pts',(-23.8985511100151,26.7541266273919,28.0263388569363));
#54401=CARTESIAN_POINT('Ctrl Pts',(-23.9004263388629,26.7539222127928,28.0264560857029));
#54402=CARTESIAN_POINT('Ctrl Pts',(-23.9043411688434,26.7534919873775,28.0267006442483));
#54403=CARTESIAN_POINT('Ctrl Pts',(-23.9063807296153,26.7532658754233,28.0268279564431));
#54404=CARTESIAN_POINT('Ctrl Pts',(-23.9117053255158,26.7526704257474,28.0271600705618));
#54405=CARTESIAN_POINT('Ctrl Pts',(-23.9149900214695,26.7522979801692,28.0273646958347));
#54406=CARTESIAN_POINT('Ctrl Pts',(-23.9292471857311,26.7506591641407,28.0282517923214));
#54407=CARTESIAN_POINT('Ctrl Pts',(-23.9402138468028,26.7493414241583,28.0289313829262));
#54408=CARTESIAN_POINT('Ctrl Pts',(-24.0195531153669,26.7393940727527,28.0338293012803));
#54409=CARTESIAN_POINT('Ctrl Pts',(-24.0876458425578,26.7286289800014,28.0379327139359));
#54410=CARTESIAN_POINT('Ctrl Pts',(-24.3309593280151,26.6821179906193,28.0524016189829));
#54411=CARTESIAN_POINT('Ctrl Pts',(-24.503489002333,26.6339897746306,28.0623096760968));
#54412=CARTESIAN_POINT('Ctrl Pts',(-24.7565693948789,26.5401050906481,28.0774020635333));
#54413=CARTESIAN_POINT('Ctrl Pts',(-24.8406071326346,26.5048088218857,28.0825098420656));
#54414=CARTESIAN_POINT('Ctrl Pts',(-25.0694713882489,26.3970558008127,28.0968979991911));
#54415=CARTESIAN_POINT('Ctrl Pts',(-25.2104861373816,26.3171872738515,28.106329339487));
#54416=CARTESIAN_POINT('Ctrl Pts',(-25.3543227497192,26.2207538054779,28.1168612304858));
#54417=CARTESIAN_POINT('Ctrl Pts',(-25.3637172506223,26.2143831803063,28.1175534212066));
#54418=CARTESIAN_POINT('Ctrl Pts',(-25.3767219573451,26.205463733545,28.1185177012015));
#54419=CARTESIAN_POINT('Ctrl Pts',(-25.3803609488482,26.2029568632052,28.1187881935831));
#54420=CARTESIAN_POINT('Ctrl Pts',(-25.3866182268595,26.1986272736532,28.1192544618639));
#54421=CARTESIAN_POINT('Ctrl Pts',(-25.3892389910645,26.1968081314066,28.1194501010067));
#54422=CARTESIAN_POINT('Ctrl Pts',(-25.3945853837571,26.1930852820729,28.1198499247448));
#54423=CARTESIAN_POINT('Ctrl Pts',(-25.3973107751573,26.1911812434922,28.1200541218613));
#54424=CARTESIAN_POINT('Ctrl Pts',(-25.4036130570688,26.1867637562282,28.1205272014696));
#54425=CARTESIAN_POINT('Ctrl Pts',(-25.4071877831266,26.1842472442549,28.1207962013687));
#54426=CARTESIAN_POINT('Ctrl Pts',(-25.4146910594564,26.1789422714237,28.1213622290977));
#54427=CARTESIAN_POINT('Ctrl Pts',(-25.418618496742,26.1761522616551,28.1216593162361));
#54428=CARTESIAN_POINT('Ctrl Pts',(-25.429043132077,26.1687114841615,28.1224500467262));
#54429=CARTESIAN_POINT('Ctrl Pts',(-25.4355292843739,26.1640453639212,28.1229442831443));
#54430=CARTESIAN_POINT('Ctrl Pts',(-25.4550701198176,26.1498771647519,28.1244401197117));
#54431=CARTESIAN_POINT('Ctrl Pts',(-25.4680706576172,26.1403011600784,28.1254445882186));
#54432=CARTESIAN_POINT('Ctrl Pts',(-25.5143256003552,26.1056912573388,28.1290521635529));
#54433=CARTESIAN_POINT('Ctrl Pts',(-25.54716513671,26.0801121891812,28.1316765383227));
#54434=CARTESIAN_POINT('Ctrl Pts',(-25.6539921234378,25.9935273870365,28.1404284164067));
#54435=CARTESIAN_POINT('Ctrl Pts',(-25.7257470106641,25.9298603046134,28.1466592813762));
#54436=CARTESIAN_POINT('Ctrl Pts',(-26.0405039909782,25.624431322755,28.1756295020245));
#54437=CARTESIAN_POINT('Ctrl Pts',(-26.2467880640397,25.3480961729768,28.1996663752747));
#54438=CARTESIAN_POINT('Ctrl Pts',(-26.406729441681,25.04245306913,28.2214696359326));
#54439=CARTESIAN_POINT('Ctrl Pts',(-26.4077864740024,25.0404278736668,28.2216139004194));
#54440=CARTESIAN_POINT('Ctrl Pts',(-26.4147549113325,25.0270421865883,28.2225660709243));
#54441=CARTESIAN_POINT('Ctrl Pts',(-26.42060082395,25.0156474484278,28.2233701672264));
#54442=CARTESIAN_POINT('Ctrl Pts',(-26.4280054483736,25.0010001710707,28.2243952512185));
#54443=CARTESIAN_POINT('Ctrl Pts',(-26.4296267326283,24.9977796554166,28.2246201114467));
#54444=CARTESIAN_POINT('Ctrl Pts',(-26.4322016269598,24.9926434474689,28.2249778814319));
#54445=CARTESIAN_POINT('Ctrl Pts',(-26.4331587335785,24.9907295265862,28.2251110114785));
#54446=CARTESIAN_POINT('Ctrl Pts',(-26.4349396884712,24.9871592761091,28.2253590035628));
#54447=CARTESIAN_POINT('Ctrl Pts',(-26.4357640113947,24.9855032014946,28.2254738951025));
#54448=CARTESIAN_POINT('Ctrl Pts',(-26.4376219591748,24.9817624917573,28.2257330935293));
#54449=CARTESIAN_POINT('Ctrl Pts',(-26.4386547504618,24.9796774507473,28.2258773472474));
#54450=CARTESIAN_POINT('Ctrl Pts',(-26.4417085436379,24.9734955054955,28.2263043953378));
#54451=CARTESIAN_POINT('Ctrl Pts',(-26.4437231044671,24.969395398564,28.2265867848962));
#54452=CARTESIAN_POINT('Ctrl Pts',(-26.4596666624731,24.9367714115786,28.2288271163122));
#54453=CARTESIAN_POINT('Ctrl Pts',(-26.4731828875898,24.9080461494892,28.2307596483457));
#54454=CARTESIAN_POINT('Ctrl Pts',(-26.5264544089083,24.7903476218444,28.2385347905647));
#54455=CARTESIAN_POINT('Ctrl Pts',(-26.5625924098078,24.6997852490306,28.2441886538635));
#54456=CARTESIAN_POINT('Ctrl Pts',(-26.7126483907092,24.2677907903654,28.2702539828218));
#54457=CARTESIAN_POINT('Ctrl Pts',(-26.7729482783921,23.910546254642,28.2895550119449));
#54458=CARTESIAN_POINT('Ctrl Pts',(-26.7730024951077,23.5507381430868,28.3112187782627));
#54459=CARTESIAN_POINT('Ctrl Pts',(-22.0750360153802,26.4155367745738,29.1557101328919));
#54460=CARTESIAN_POINT('Ctrl Pts',(-21.903523834291,26.3272322362299,29.1428205289804));
#54461=CARTESIAN_POINT('Ctrl Pts',(-21.7402616852622,26.2236941082807,29.1302936435899));
#54462=CARTESIAN_POINT('Ctrl Pts',(-21.5770994734328,26.0983787718882,29.117532731908));
#54463=CARTESIAN_POINT('Ctrl Pts',(-21.5670275385601,26.0905475857023,29.1167437886155));
#54464=CARTESIAN_POINT('Ctrl Pts',(-21.5533519097916,26.0797835255595,29.1156708205667));
#54465=CARTESIAN_POINT('Ctrl Pts',(-21.5497077664611,26.0769024451824,29.1153847364847));
#54466=CARTESIAN_POINT('Ctrl Pts',(-21.5435228987184,26.0719908845966,29.1148988971793));
#54467=CARTESIAN_POINT('Ctrl Pts',(-21.5409790027695,26.0699644252359,29.114698981506));
#54468=CARTESIAN_POINT('Ctrl Pts',(-21.5358594045649,26.0658734864667,29.1142964764718));
#54469=CARTESIAN_POINT('Ctrl Pts',(-21.5332837974685,26.0638088935059,29.1140938919889));
#54470=CARTESIAN_POINT('Ctrl Pts',(-21.5274384342904,26.0591085116993,29.1136339193165));
#54471=CARTESIAN_POINT('Ctrl Pts',(-21.5241706447973,26.0564702774051,29.1133766298839));
#54472=CARTESIAN_POINT('Ctrl Pts',(-21.5173501630926,26.0509417361898,29.1128393073652));
#54473=CARTESIAN_POINT('Ctrl Pts',(-21.5137984538577,26.0480502270551,29.1125593234604));
#54474=CARTESIAN_POINT('Ctrl Pts',(-21.5045092149839,26.0404547104572,29.1118265708541));
#54475=CARTESIAN_POINT('Ctrl Pts',(-21.4987817218802,26.0357384252181,29.111374298945));
#54476=CARTESIAN_POINT('Ctrl Pts',(-21.4818351742594,26.0216853626285,29.1100346517203));
#54477=CARTESIAN_POINT('Ctrl Pts',(-21.4706631048166,26.0122920173259,29.109149573495));
#54478=CARTESIAN_POINT('Ctrl Pts',(-21.3506622089354,25.9099970694466,29.0996207145988));
#54479=CARTESIAN_POINT('Ctrl Pts',(-21.2480643489262,25.8100156362744,29.0912864711653));
#54480=CARTESIAN_POINT('Ctrl Pts',(-21.0312821028377,25.5686152585135,29.0728030485355));
#54481=CARTESIAN_POINT('Ctrl Pts',(-20.9217277054565,25.4237139561571,29.0628036964094));
#54482=CARTESIAN_POINT('Ctrl Pts',(-20.760844296867,25.1688138446026,29.0458442317717));
#54483=CARTESIAN_POINT('Ctrl Pts',(-20.7024796284295,25.0637660794743,29.0390054648641));
#54484=CARTESIAN_POINT('Ctrl Pts',(-20.6281524228337,24.9103941499232,29.0288923486045));
#54485=CARTESIAN_POINT('Ctrl Pts',(-20.6072545609322,24.864564715976,29.02585461993));
#54486=CARTESIAN_POINT('Ctrl Pts',(-20.5854302267779,24.8135705309798,29.022437150822));
#54487=CARTESIAN_POINT('Ctrl Pts',(-20.5834311389967,24.8088686328279,29.0221216983338));
#54488=CARTESIAN_POINT('Ctrl Pts',(-20.5804726977639,24.8018641020228,29.0216512180069));
#54489=CARTESIAN_POINT('Ctrl Pts',(-20.5795048107722,24.7995650480557,29.0214967082355));
#54490=CARTESIAN_POINT('Ctrl Pts',(-20.5778492254366,24.7956196786666,29.0212314036766));
#54491=CARTESIAN_POINT('Ctrl Pts',(-20.5771602214079,24.7939739073594,29.0211206889759));
#54492=CARTESIAN_POINT('Ctrl Pts',(-20.5758165103108,24.7907567900429,29.0209041757315));
#54493=CARTESIAN_POINT('Ctrl Pts',(-20.5751616831767,24.7891855013489,29.0207983850234));
#54494=CARTESIAN_POINT('Ctrl Pts',(-20.5735772191261,24.7853750051121,29.0205417325251));
#54495=CARTESIAN_POINT('Ctrl Pts',(-20.572648865471,24.7831352704797,29.0203907921514));
#54496=CARTESIAN_POINT('Ctrl Pts',(-20.5697912283803,24.7762189157929,29.0199244269508));
#54497=CARTESIAN_POINT('Ctrl Pts',(-20.5678704406278,24.7715388280006,29.0196084884382));
#54498=CARTESIAN_POINT('Ctrl Pts',(-20.5463318034568,24.7187051218155,29.0160379120575));
#54499=CARTESIAN_POINT('Ctrl Pts',(-20.5278724415341,24.670091362248,29.0127157923183));
#54500=CARTESIAN_POINT('Ctrl Pts',(-20.4826350647755,24.5416775352006,29.0038842426427));
#54501=CARTESIAN_POINT('Ctrl Pts',(-20.4577937627476,24.4612394751727,28.9982970890804));
#54502=CARTESIAN_POINT('Ctrl Pts',(-20.4127050062616,24.2920023094964,28.9865466057507));
#54503=CARTESIAN_POINT('Ctrl Pts',(-20.393014293255,24.2031256870088,28.9803787235144));
#54504=CARTESIAN_POINT('Ctrl Pts',(-20.3600394111265,24.0173687267186,28.9676101963295));
#54505=CARTESIAN_POINT('Ctrl Pts',(-20.3473480346287,23.9204707371898,28.9610177853943));
#54506=CARTESIAN_POINT('Ctrl Pts',(-20.3235423274876,23.6403421778372,28.9422828299221));
#54507=CARTESIAN_POINT('Ctrl Pts',(-20.3236426732886,23.4565248657216,28.9304058818221));
#54508=CARTESIAN_POINT('Ctrl Pts',(-20.3403899451264,23.2620944636847,28.9183109226904));
#54509=CARTESIAN_POINT('Ctrl Pts',(-20.3414510464762,23.2505094233887,28.9175919064636));
#54510=CARTESIAN_POINT('Ctrl Pts',(-20.3430059568645,23.234488560877,28.9165998177692));
#54511=CARTESIAN_POINT('Ctrl Pts',(-20.3434462743388,23.2300477454694,28.9163250587344));
#54512=CARTESIAN_POINT('Ctrl Pts',(-20.34421811424,23.2224246605355,28.9158538119853));
#54513=CARTESIAN_POINT('Ctrl Pts',(-20.3445451533826,23.2192419521463,28.9156571829187));
#54514=CARTESIAN_POINT('Ctrl Pts',(-20.3452205942789,23.2127635308989,28.9152571872378));
#54515=CARTESIAN_POINT('Ctrl Pts',(-20.3455693412412,23.2094678570523,28.9150538317693));
#54516=CARTESIAN_POINT('Ctrl Pts',(-20.346384134712,23.2018798889987,28.9145859190452));
#54517=CARTESIAN_POINT('Ctrl Pts',(-20.3468537250986,23.1975879749979,28.9143214740985));
#54518=CARTESIAN_POINT('Ctrl Pts',(-20.3478581222631,23.188575635692,28.9137666304346));
#54519=CARTESIAN_POINT('Ctrl Pts',(-20.3483947448019,23.1838554198682,28.9134762896437));
#54520=CARTESIAN_POINT('Ctrl Pts',(-20.3498438792451,23.1713549406675,28.9127080601571));
#54521=CARTESIAN_POINT('Ctrl Pts',(-20.350774328509,23.1635767551045,28.9122307379048));
#54522=CARTESIAN_POINT('Ctrl Pts',(-20.3536577931424,23.1401953258242,28.9107979297246));
#54523=CARTESIAN_POINT('Ctrl Pts',(-20.3556966760933,23.124602753586,28.9098451497913));
#54524=CARTESIAN_POINT('Ctrl Pts',(-20.363351001329,23.0692215348088,28.9064702502806));
#54525=CARTESIAN_POINT('Ctrl Pts',(-20.3695964940952,23.0295226892218,28.9040679124913));
#54526=CARTESIAN_POINT('Ctrl Pts',(-20.3922646563213,22.9011256034451,28.8963427179516));
#54527=CARTESIAN_POINT('Ctrl Pts',(-20.4116691199122,22.812994580749,28.8911110161058));
#54528=CARTESIAN_POINT('Ctrl Pts',(-20.4775906594915,22.5638887167067,28.8763834340805));
#54529=CARTESIAN_POINT('Ctrl Pts',(-20.5329888601922,22.4055750358515,28.8671078768767));
#54530=CARTESIAN_POINT('Ctrl Pts',(-20.6756630740369,22.0813292410139,28.8472642605691));
#54531=CARTESIAN_POINT('Ctrl Pts',(-20.7655918131333,21.9172667594246,28.836703385407));
#54532=CARTESIAN_POINT('Ctrl Pts',(-20.8755459019558,21.7524224762358,28.8245734898339));
#54533=CARTESIAN_POINT('Ctrl Pts',(-20.8819451783495,21.7429384133756,28.8238699021014));
#54534=CARTESIAN_POINT('Ctrl Pts',(-20.8903618471657,21.7306066085806,28.8229472878342));
#54535=CARTESIAN_POINT('Ctrl Pts',(-20.8923336576871,21.7277276352751,28.8227313396326));
#54536=CARTESIAN_POINT('Ctrl Pts',(-20.8953764826729,21.7233003508187,28.8223983891156));
#54537=CARTESIAN_POINT('Ctrl Pts',(-20.896444192349,21.721749754871,28.822281613928));
#54538=CARTESIAN_POINT('Ctrl Pts',(-20.8985720327129,21.7186653592511,28.822049000321));
#54539=CARTESIAN_POINT('Ctrl Pts',(-20.8996321318709,21.7171315496222,28.8219331640678));
#54540=CARTESIAN_POINT('Ctrl Pts',(-20.9020019416855,21.7137091324778,28.8216743351153));
#54541=CARTESIAN_POINT('Ctrl Pts',(-20.9033123392048,21.7118210094471,28.8215312951069));
#54542=CARTESIAN_POINT('Ctrl Pts',(-20.9071541521064,21.7062980478469,28.8211121712726));
#54543=CARTESIAN_POINT('Ctrl Pts',(-20.9096910298006,21.7026670433236,28.8208357134777));
#54544=CARTESIAN_POINT('Ctrl Pts',(-20.9283225649299,21.6761166914224,28.8188076175202));
#54545=CARTESIAN_POINT('Ctrl Pts',(-20.9447072428868,21.6534036933718,28.8170365525425));
#54546=CARTESIAN_POINT('Ctrl Pts',(-20.9991043040542,21.580031361701,28.8112042151842));
#54547=CARTESIAN_POINT('Ctrl Pts',(-21.0383124309599,21.530281116342,28.807073907356));
#54548=CARTESIAN_POINT('Ctrl Pts',(-21.233359575192,21.2972562751459,28.7869896314095));
#54549=CARTESIAN_POINT('Ctrl Pts',(-21.4079290619932,21.1306567553353,28.7704254561559));
#54550=CARTESIAN_POINT('Ctrl Pts',(-21.7409514727248,20.8773957308274,28.74259042454));
#54551=CARTESIAN_POINT('Ctrl Pts',(-21.8911660006027,20.7816454824267,28.7310968101406));
#54552=CARTESIAN_POINT('Ctrl Pts',(-22.0587419710486,20.6933929337504,28.7193592112775));
#54553=CARTESIAN_POINT('Ctrl Pts',(-22.0689730128347,20.6880747756077,28.7186465676134));
#54554=CARTESIAN_POINT('Ctrl Pts',(-22.0831916387644,20.6807805072414,28.7176616028229));
#54555=CARTESIAN_POINT('Ctrl Pts',(-22.0871550108788,20.6787576235368,28.7173876309787));
#54556=CARTESIAN_POINT('Ctrl Pts',(-22.0939751372373,20.6752944540647,28.7169171786178));
#54557=CARTESIAN_POINT('Ctrl Pts',(-22.0968298625359,20.6738502054134,28.716720558636));
#54558=CARTESIAN_POINT('Ctrl Pts',(-22.1026531368747,20.6709150055017,28.7163200859506));
#54559=CARTESIAN_POINT('Ctrl Pts',(-22.1056218508138,20.6694243879801,28.7161162451546));
#54560=CARTESIAN_POINT('Ctrl Pts',(-22.1124810333354,20.665993600724,28.715646010426));
#54561=CARTESIAN_POINT('Ctrl Pts',(-22.1163731397596,20.664056704649,28.7153797316374));
#54562=CARTESIAN_POINT('Ctrl Pts',(-22.1245568069852,20.6600047648638,28.7148209864917));
#54563=CARTESIAN_POINT('Ctrl Pts',(-22.1288491854022,20.6578913888459,28.7145285788996));
#54564=CARTESIAN_POINT('Ctrl Pts',(-22.1402496684181,20.6523098060472,28.7137536813049));
#54565=CARTESIAN_POINT('Ctrl Pts',(-22.1473658916364,20.6488581785474,28.7132717693729));
#54566=CARTESIAN_POINT('Ctrl Pts',(-22.1688461923039,20.6385369544802,28.7118224247145));
#54567=CARTESIAN_POINT('Ctrl Pts',(-22.1832486855846,20.6317475075697,28.7108577665009));
#54568=CARTESIAN_POINT('Ctrl Pts',(-22.2347717001149,20.6079242396428,28.7074315572543));
#54569=CARTESIAN_POINT('Ctrl Pts',(-22.2721659447374,20.5914891925991,28.7049904304417));
#54570=CARTESIAN_POINT('Ctrl Pts',(-22.395497582566,20.5400586959942,28.6970759881295));
#54571=CARTESIAN_POINT('Ctrl Pts',(-22.482637844172,20.5080614020839,28.6916994293299));
#54572=CARTESIAN_POINT('Ctrl Pts',(-22.7323780904471,20.4284140801791,28.6767321366502));
#54573=CARTESIAN_POINT('Ctrl Pts',(-22.8975169296546,20.3897570278578,28.6673595754364));
#54574=CARTESIAN_POINT('Ctrl Pts',(-23.173533396809,20.3477116210626,28.6517015382719));
#54575=CARTESIAN_POINT('Ctrl Pts',(-23.2829031045341,20.336733173535,28.6454940292578));
#54576=CARTESIAN_POINT('Ctrl Pts',(-23.4031759185237,20.330842973238,28.6384708234775));
#54577=CARTESIAN_POINT('Ctrl Pts',(-23.413742622887,20.3303776155765,28.6378521161621));
#54578=CARTESIAN_POINT('Ctrl Pts',(-23.4416478732878,20.3292862781204,28.6362133299423));
#54579=CARTESIAN_POINT('Ctrl Pts',(-23.4589892964726,20.3287482902693,28.6351899687757));
#54580=CARTESIAN_POINT('Ctrl Pts',(-23.4835473303668,20.3281848663916,28.6337326745831));
#54581=CARTESIAN_POINT('Ctrl Pts',(-23.4907612490409,20.3280435984958,28.6333036098166));
#54582=CARTESIAN_POINT('Ctrl Pts',(-23.5007481657472,20.327881576971,28.6327081770578));
#54583=CARTESIAN_POINT('Ctrl Pts',(-23.5035208595915,20.3278401740327,28.6325427121346));
#54584=CARTESIAN_POINT('Ctrl Pts',(-23.5118229809335,20.3277269209445,28.6320468014854));
#54585=CARTESIAN_POINT('Ctrl Pts',(-23.5173525145251,20.3276657244335,28.6317158838186));
#54586=CARTESIAN_POINT('Ctrl Pts',(-23.5588418223804,20.3273133484892,28.6292280872079));
#54587=CARTESIAN_POINT('Ctrl Pts',(-23.5948022662794,20.3276098566029,28.6270444895093));
#54588=CARTESIAN_POINT('Ctrl Pts',(-23.6354010396643,20.3286242236627,28.6245408345939));
#54589=CARTESIAN_POINT('Ctrl Pts',(-23.6400534359174,20.3287505496246,28.6242533595278));
#54590=CARTESIAN_POINT('Ctrl Pts',(-23.64708555455,20.3289567368816,28.6238179560723));
#54591=CARTESIAN_POINT('Ctrl Pts',(-23.6494655143603,20.3290291591263,28.6236704445302));
#54592=CARTESIAN_POINT('Ctrl Pts',(-23.6536001914156,20.3291595640591,28.6234139052064));
#54593=CARTESIAN_POINT('Ctrl Pts',(-23.6553549495317,20.3292163433464,28.6233049455962));
#54594=CARTESIAN_POINT('Ctrl Pts',(-23.6590232801263,20.3293380415569,28.6230769872293));
#54595=CARTESIAN_POINT('Ctrl Pts',(-23.6609368369518,20.3294032317447,28.6229579731648));
#54596=CARTESIAN_POINT('Ctrl Pts',(-23.6655068015381,20.3295629966305,28.6226735029309));
#54597=CARTESIAN_POINT('Ctrl Pts',(-23.6681631495431,20.3296591525073,28.6225079572129));
#54598=CARTESIAN_POINT('Ctrl Pts',(-23.6771363786964,20.3299950866329,28.6219480903426));
#54599=CARTESIAN_POINT('Ctrl Pts',(-23.6834526203049,20.3302501624584,28.6215529158448));
#54600=CARTESIAN_POINT('Ctrl Pts',(-23.69844443881,20.3308997795109,28.6206124449374));
#54601=CARTESIAN_POINT('Ctrl Pts',(-23.7071192002536,20.331310806751,28.6200662610029));
#54602=CARTESIAN_POINT('Ctrl Pts',(-23.8083774813217,20.3365189075832,28.6136683136895));
#54603=CARTESIAN_POINT('Ctrl Pts',(-23.900705019942,20.3452733203515,28.6076161065517));
#54604=CARTESIAN_POINT('Ctrl Pts',(-24.0779979398687,20.3698359415566,28.5957272710955));
#54605=CARTESIAN_POINT('Ctrl Pts',(-24.1629661174933,20.385107063928,28.5899091368595));
#54606=CARTESIAN_POINT('Ctrl Pts',(-24.2746459259265,20.4098447362447,28.5821724059398));
#54607=CARTESIAN_POINT('Ctrl Pts',(-24.3019957300885,20.4162791639482,28.5802703940746));
#54608=CARTESIAN_POINT('Ctrl Pts',(-24.4234252096127,20.4465281885524,28.5717997830398));
#54609=CARTESIAN_POINT('Ctrl Pts',(-24.5164880137386,20.4742282232915,28.5652402726388));
#54610=CARTESIAN_POINT('Ctrl Pts',(-24.7905098614222,20.5694563368348,28.5458600719231));
#54611=CARTESIAN_POINT('Ctrl Pts',(-24.9668212259242,20.6490903843892,28.5333300852608));
#54612=CARTESIAN_POINT('Ctrl Pts',(-25.1453912938353,20.7499323514752,28.5206168217921));
#54613=CARTESIAN_POINT('Ctrl Pts',(-25.1557791801157,20.7558751467224,28.5198770302077));
#54614=CARTESIAN_POINT('Ctrl Pts',(-25.1700441836802,20.7641418029993,28.5188607440423));
#54615=CARTESIAN_POINT('Ctrl Pts',(-25.1739497755004,20.7664161052546,28.5185824573165));
#54616=CARTESIAN_POINT('Ctrl Pts',(-25.1806272135395,20.7703233403922,28.5181065948648));
#54617=CARTESIAN_POINT('Ctrl Pts',(-25.1834014150319,20.7719522173232,28.517908872133));
#54618=CARTESIAN_POINT('Ctrl Pts',(-25.1890264565541,20.7752663059936,28.5175079189169));
#54619=CARTESIAN_POINT('Ctrl Pts',(-25.1918771479565,20.7769517638287,28.5173046976849));
#54620=CARTESIAN_POINT('Ctrl Pts',(-25.1984113926356,20.7808287102722,28.5168388244732));
#54621=CARTESIAN_POINT('Ctrl Pts',(-25.2020931876752,20.783023162616,28.5165762809616));
#54622=CARTESIAN_POINT('Ctrl Pts',(-25.2098041424527,20.7876399791569,28.5160263304025));
#54623=CARTESIAN_POINT('Ctrl Pts',(-25.2138324043022,20.790063829444,28.5157389783342));
#54624=CARTESIAN_POINT('Ctrl Pts',(-25.2244539619891,20.7964866382278,28.514981148636));
#54625=CARTESIAN_POINT('Ctrl Pts',(-25.2310382613092,20.8005004777874,28.5145112158891));
#54626=CARTESIAN_POINT('Ctrl Pts',(-25.2507165486983,20.8125936023207,28.5131062290394));
#54627=CARTESIAN_POINT('Ctrl Pts',(-25.2637672765258,20.820743140133,28.5121737523546));
#54628=CARTESIAN_POINT('Ctrl Pts',(-25.30969697711,20.8498832251091,28.5088891248205));
#54629=CARTESIAN_POINT('Ctrl Pts',(-25.3422535152869,20.8713774283177,28.5065555449449));
#54630=CARTESIAN_POINT('Ctrl Pts',(-25.4444341715162,20.9415348712261,28.4992051808918));
#54631=CARTESIAN_POINT('Ctrl Pts',(-25.5125308931006,20.9923633248121,28.4942679563359));
#54632=CARTESIAN_POINT('Ctrl Pts',(-25.706029638216,21.1490745983631,28.4800010846273));
#54633=CARTESIAN_POINT('Ctrl Pts',(-25.8254496385929,21.2619100678056,28.4708949956884));
#54634=CARTESIAN_POINT('Ctrl Pts',(-26.0678445978434,21.5287584565743,28.4507224526013));
#54635=CARTESIAN_POINT('Ctrl Pts',(-26.1863370045312,21.6859184357703,28.4396635085306));
#54636=CARTESIAN_POINT('Ctrl Pts',(-26.2960923857667,21.8630580610241,28.4269138152973));
#54637=CARTESIAN_POINT('Ctrl Pts',(-26.3023582224796,21.8732981667442,28.4261757877939));
#54638=CARTESIAN_POINT('Ctrl Pts',(-26.3104067073467,21.8866182120766,28.4252141775191));
#54639=CARTESIAN_POINT('Ctrl Pts',(-26.3122417765848,21.8896666008855,28.4249939976785));
#54640=CARTESIAN_POINT('Ctrl Pts',(-26.3150478628767,21.8943455473509,28.4246558695367));
#54641=CARTESIAN_POINT('Ctrl Pts',(-26.3160225016005,21.8959739464359,28.424538159247));
#54642=CARTESIAN_POINT('Ctrl Pts',(-26.317942377159,21.8991880599697,28.4243057579234));
#54643=CARTESIAN_POINT('Ctrl Pts',(-26.3188876861248,21.9007737194376,28.4241910724519));
#54644=CARTESIAN_POINT('Ctrl Pts',(-26.3209914087059,21.9043094031452,28.4239352770239));
#54645=CARTESIAN_POINT('Ctrl Pts',(-26.3221491216886,21.9062598305841,28.4237941218961));
#54646=CARTESIAN_POINT('Ctrl Pts',(-26.3254898856854,21.911901658492,28.4233856802544));
#54647=CARTESIAN_POINT('Ctrl Pts',(-26.3276676177528,21.9155961782255,28.4231180479484));
#54648=CARTESIAN_POINT('Ctrl Pts',(-26.3423891219573,21.9406855370152,28.421299496154));
#54649=CARTESIAN_POINT('Ctrl Pts',(-26.3546924900912,21.9622194473466,28.4197333885703));
#54650=CARTESIAN_POINT('Ctrl Pts',(-26.3919649537566,22.029239562356,28.4148481064973));
#54651=CARTESIAN_POINT('Ctrl Pts',(-26.4160838760334,22.0751864403287,28.4114834061322));
#54652=CARTESIAN_POINT('Ctrl Pts',(-26.4589273314549,22.1618243229434,28.4051371508418));
#54653=CARTESIAN_POINT('Ctrl Pts',(-26.4779338747275,22.2023639469,28.4021669150757));
#54654=CARTESIAN_POINT('Ctrl Pts',(-26.642684599646,22.5737033947311,28.3750302911328));
#54655=CARTESIAN_POINT('Ctrl Pts',(-26.7326952720963,22.926570046644,28.3501549653898));
#54656=CARTESIAN_POINT('Ctrl Pts',(-26.7638871041612,23.307189710949,28.326181623642));
#54657=CARTESIAN_POINT('Ctrl Pts',(-26.7653493835414,23.3273647492704,28.32491783057));
#54658=CARTESIAN_POINT('Ctrl Pts',(-26.7676781248179,23.3643163718506,28.3226155081313));
#54659=CARTESIAN_POINT('Ctrl Pts',(-26.7686035406181,23.3810884002205,28.3215751632675));
#54660=CARTESIAN_POINT('Ctrl Pts',(-26.7696713833718,23.4036466079819,28.3201820081312));
#54661=CARTESIAN_POINT('Ctrl Pts',(-26.769929403328,23.4094268154008,28.3198255704294));
#54662=CARTESIAN_POINT('Ctrl Pts',(-26.7703096151641,23.4184923351576,28.3192673774902));
#54663=CARTESIAN_POINT('Ctrl Pts',(-26.7704423478823,23.4217771720332,28.3190652913293));
#54664=CARTESIAN_POINT('Ctrl Pts',(-26.770697704254,23.4283457999143,28.318661524494));
#54665=CARTESIAN_POINT('Ctrl Pts',(-26.7708203322258,23.4316295869276,28.3184598439135));
#54666=CARTESIAN_POINT('Ctrl Pts',(-26.7710536577081,23.4381448870054,28.318060029171));
#54667=CARTESIAN_POINT('Ctrl Pts',(-26.7711645148531,23.441376390166,28.3178618902309));
#54668=CARTESIAN_POINT('Ctrl Pts',(-26.7714045286842,23.4486942259397,28.3174135673003));
#54669=CARTESIAN_POINT('Ctrl Pts',(-26.7715307733969,23.4527806539243,28.3171634749366));
#54670=CARTESIAN_POINT('Ctrl Pts',(-26.7718304723853,23.4631190081454,28.316531412623));
#54671=CARTESIAN_POINT('Ctrl Pts',(-26.7719935045567,23.4693712389252,28.3161497697238));
#54672=CARTESIAN_POINT('Ctrl Pts',(-26.7727181990729,23.5006579469635,28.3142429716697));
#54673=CARTESIAN_POINT('Ctrl Pts',(-26.7730062814916,23.5256982728467,28.3127264089526));
#54674=CARTESIAN_POINT('Ctrl Pts',(-26.7730024948489,23.5507398571939,28.3112186750576));
#54675=CARTESIAN_POINT('Origin',(-23.5502525316942,23.5502525316942,0.));
#54676=CARTESIAN_POINT('',(-27.4844229589094,23.5526670019077,-74.5958360648399));
#54677=CARTESIAN_POINT('',(-21.8015553287927,27.0731131722198,-74.9999401439847));
#54678=CARTESIAN_POINT('Ctrl Pts',(-27.4832517860125,23.5526744176369,-74.5958364779651));
#54679=CARTESIAN_POINT('Ctrl Pts',(-27.483176366467,23.6751512902655,-74.6020627797075));
#54680=CARTESIAN_POINT('Ctrl Pts',(-27.4773804143339,23.7974636017587,-74.6082890814499));
#54681=CARTESIAN_POINT('Ctrl Pts',(-27.4659067048209,23.9192259676967,-74.6145153831923));
#54682=CARTESIAN_POINT('Ctrl Pts',(-27.4550637875768,24.0342941813215,-74.620399380382));
#54683=CARTESIAN_POINT('Ctrl Pts',(-27.4391265096654,24.149073567767,-74.6262833775717));
#54684=CARTESIAN_POINT('Ctrl Pts',(-27.4181161321085,24.2630780142565,-74.6321673747614));
#54685=CARTESIAN_POINT('Ctrl Pts',(-27.3971330386182,24.3769344146246,-74.638043730995));
#54686=CARTESIAN_POINT('Ctrl Pts',(-27.3710900215547,24.4900174753001,-74.6439200872287));
#54687=CARTESIAN_POINT('Ctrl Pts',(-27.3400601821272,24.6018451204468,-74.6497964434623));
#54688=CARTESIAN_POINT('Ctrl Pts',(-27.3090624249359,24.7135571452428,-74.6556667240394));
#54689=CARTESIAN_POINT('Ctrl Pts',(-27.2730882110991,24.8240159422074,-74.6615370046165));
#54690=CARTESIAN_POINT('Ctrl Pts',(-27.2322617585231,24.9327492056673,-74.6674072851936));
#54691=CARTESIAN_POINT('Ctrl Pts',(-27.1899550191757,25.0454249231332,-74.6734904105842));
#54692=CARTESIAN_POINT('Ctrl Pts',(-27.142437582367,25.1562471619655,-74.6795735359748));
#54693=CARTESIAN_POINT('Ctrl Pts',(-27.0899044923739,25.2647066714297,-74.6856566613653));
#54694=CARTESIAN_POINT('Ctrl Pts',(-27.039269673959,25.3692470205281,-74.6915199743665));
#54695=CARTESIAN_POINT('Ctrl Pts',(-26.9839755999771,25.4715920343096,-74.6973832873676));
#54696=CARTESIAN_POINT('Ctrl Pts',(-26.9242457874241,25.5713063435184,-74.7032466003688));
#54697=CARTESIAN_POINT('Ctrl Pts',(-26.864525935161,25.6710040247924,-74.7091089356287));
#54698=CARTESIAN_POINT('Ctrl Pts',(-26.8003720267301,25.7680715208646,-74.7149712708887));
#54699=CARTESIAN_POINT('Ctrl Pts',(-26.7320527052678,25.8620995541953,-74.7208336061487));
#54700=CARTESIAN_POINT('Ctrl Pts',(-26.6637284033848,25.95613444209,-74.7266963687679));
#54701=CARTESIAN_POINT('Ctrl Pts',(-26.591238326868,26.0471290938028,-74.7325591313872));
#54702=CARTESIAN_POINT('Ctrl Pts',(-26.5148930582176,26.1347051910584,-74.7384218940064));
#54703=CARTESIAN_POINT('Ctrl Pts',(-26.4385239277329,26.2223086603617,-74.7442864890414));
#54704=CARTESIAN_POINT('Ctrl Pts',(-26.3582974793948,26.306491140376,-74.7501510840764));
#54705=CARTESIAN_POINT('Ctrl Pts',(-26.2745625120793,26.3869097423515,-74.7560156791114));
#54706=CARTESIAN_POINT('Ctrl Pts',(-26.1907356370096,26.4674166120286,-74.7618867111437));
#54707=CARTESIAN_POINT('Ctrl Pts',(-26.1033928533998,26.5441510722657,-74.7677577431759));
#54708=CARTESIAN_POINT('Ctrl Pts',(-26.0129176017944,26.6168091922678,-74.7736287752082));
#54709=CARTESIAN_POINT('Ctrl Pts',(-25.922383302987,26.6895147314106,-74.7795036388741));
#54710=CARTESIAN_POINT('Ctrl Pts',(-25.828712796173,26.7581383894547,-74.78537850254));
#54711=CARTESIAN_POINT('Ctrl Pts',(-25.7323187762878,26.8224193832171,-74.7912533662059));
#54712=CARTESIAN_POINT('Ctrl Pts',(-25.6357870685638,26.8867921950312,-74.797136621443));
#54713=CARTESIAN_POINT('Ctrl Pts',(-25.5365244343096,26.9468097497519,-74.80301987668));
#54714=CARTESIAN_POINT('Ctrl Pts',(-25.4349684871045,27.0022569881545,-74.8089031319171));
#54715=CARTESIAN_POINT('Ctrl Pts',(-25.409080510343,27.0163912349294,-74.8104028528005));
#54716=CARTESIAN_POINT('Ctrl Pts',(-25.3830436130049,27.0302287427077,-74.811902573684));
#54717=CARTESIAN_POINT('Ctrl Pts',(-25.3568652381275,27.0437664545166,-74.8134022945674));
#54718=CARTESIAN_POINT('Ctrl Pts',(-25.2551946978962,27.0963436858972,-74.8192268514059));
#54719=CARTESIAN_POINT('Ctrl Pts',(-25.1510459488802,27.1445723874773,-74.8250514082445));
#54720=CARTESIAN_POINT('Ctrl Pts',(-25.0448307679798,27.1882086743135,-74.830875965083));
#54721=CARTESIAN_POINT('Ctrl Pts',(-24.9387513096792,27.2317892023566,-74.8366930792566));
#54722=CARTESIAN_POINT('Ctrl Pts',(-24.8306110542562,27.2707888232278,-74.8425101934303));
#54723=CARTESIAN_POINT('Ctrl Pts',(-24.720846744442,27.3050092733595,-74.848327307604));
#54724=CARTESIAN_POINT('Ctrl Pts',(-24.6111921317371,27.3391955239917,-74.8541386082248));
#54725=CARTESIAN_POINT('Ctrl Pts',(-24.4999170912857,27.3686119767027,-74.8599499088456));
#54726=CARTESIAN_POINT('Ctrl Pts',(-24.3874780220788,27.393108563118,-74.8657612094665));
#54727=CARTESIAN_POINT('Ctrl Pts',(-24.275117106024,27.417588122663,-74.87156847082));
#54728=CARTESIAN_POINT('Ctrl Pts',(-24.1615941799012,27.4371545269804,-74.8773757321735));
#54729=CARTESIAN_POINT('Ctrl Pts',(-24.0473797635603,27.4517078390554,-74.883182993527));
#54730=CARTESIAN_POINT('Ctrl Pts',(-23.9332063326367,27.4662559287287,-74.8889881709664));
#54731=CARTESIAN_POINT('Ctrl Pts',(-23.818342321467,27.4757944482308,-74.8947933484058));
#54732=CARTESIAN_POINT('Ctrl Pts',(-23.7032666959445,27.4802748809358,-74.9005985258453));
#54733=CARTESIAN_POINT('Ctrl Pts',(-23.5882033789001,27.4847548344142,-74.9064030823634));
#54734=CARTESIAN_POINT('Ctrl Pts',(-23.4729289128697,27.4841777605835,-74.9122076388816));
#54735=CARTESIAN_POINT('Ctrl Pts',(-23.3579248026403,27.4785472055491,-74.9180121953998));
#54736=CARTESIAN_POINT('Ctrl Pts',(-23.2429040244642,27.4729158344588,-74.9238175931926));
#54737=CARTESIAN_POINT('Ctrl Pts',(-23.1281541001282,27.4622295477948,-74.9296229909855));
#54738=CARTESIAN_POINT('Ctrl Pts',(-23.01415313124,27.4465439007826,-74.9354283887783));
#54739=CARTESIAN_POINT('Ctrl Pts',(-22.90003966309,27.4308427747466,-74.9412395154958));
#54740=CARTESIAN_POINT('Ctrl Pts',(-22.7866770436019,27.4101324947738,-74.9470506422132));
#54741=CARTESIAN_POINT('Ctrl Pts',(-22.674534903303,27.3845200804347,-74.9528617689307));
#54742=CARTESIAN_POINT('Ctrl Pts',(-22.5623338906578,27.3588942200983,-74.9586759463717));
#54743=CARTESIAN_POINT('Ctrl Pts',(-22.451355038326,27.3283612127694,-74.9644901238128));
#54744=CARTESIAN_POINT('Ctrl Pts',(-22.342052709662,27.2930779604367,-74.9703043012538));
#54745=CARTESIAN_POINT('Ctrl Pts',(-22.2325830393214,27.2577406895055,-74.9761273801904));
#54746=CARTESIAN_POINT('Ctrl Pts',(-22.1247954125246,27.2176387965384,-74.981950459127));
#54747=CARTESIAN_POINT('Ctrl Pts',(-22.0191243475635,27.1729774017003,-74.9877735380637));
#54748=CARTESIAN_POINT('Ctrl Pts',(-21.9455287910648,27.1418725745811,-74.9918290733707));
#54749=CARTESIAN_POINT('Ctrl Pts',(-21.8729594269255,27.1085571364925,-74.9958846086777));
#54750=CARTESIAN_POINT('Ctrl Pts',(-21.8015553287927,27.0731131722198,-74.9999401439847));
#54751=CARTESIAN_POINT('',(-25.2989470070244,27.0731145261455,-75.));
#54752=CARTESIAN_POINT('Origin',(-23.5502525316942,23.5502525316942,-75.));
#54753=CARTESIAN_POINT('',(-27.4851692780616,23.554414982299,-74.7791635220347));
#54754=CARTESIAN_POINT('Ctrl Pts',(-25.2989470070244,27.0731145261455,-75.0000000000001));
#54755=CARTESIAN_POINT('Ctrl Pts',(-26.4728992620448,26.4903826945015,-74.9337043628751));
#54756=CARTESIAN_POINT('Ctrl Pts',(-27.4161416976464,25.1461349635273,-74.8600922035533));
#54757=CARTESIAN_POINT('Ctrl Pts',(-27.4883708345099,23.69846686772,-74.7864800442315));
#54758=CARTESIAN_POINT('Ctrl Pts',(-27.4872905609711,23.5544172262436,-74.7791635220347));
#54759=CARTESIAN_POINT('',(-27.4817157848272,23.5524277069527,-73.5291635548767));
#54760=CARTESIAN_POINT('Ctrl Pts',(-27.4832503311977,23.5544129523903,-74.7791635220347));
#54761=CARTESIAN_POINT('Ctrl Pts',(-27.4833696199972,23.4416448887938,-74.7734299077509));
#54762=CARTESIAN_POINT('Ctrl Pts',(-27.4786348720723,23.3286475420881,-74.7676962934671));
#54763=CARTESIAN_POINT('Ctrl Pts',(-27.4690136201014,23.2158866662325,-74.7619626791833));
#54764=CARTESIAN_POINT('Ctrl Pts',(-27.4594043197065,23.1032658626041,-74.7562361872291));
#54765=CARTESIAN_POINT('Ctrl Pts',(-27.4449206105733,22.9908813736366,-74.750509695275));
#54766=CARTESIAN_POINT('Ctrl Pts',(-27.4255820071538,22.8792007776292,-74.7447832033208));
#54767=CARTESIAN_POINT('Ctrl Pts',(-27.4055227965739,22.7633586692614,-74.7388433272345));
#54768=CARTESIAN_POINT('Ctrl Pts',(-27.3802397965917,22.6482744033037,-74.7329034511482));
#54769=CARTESIAN_POINT('Ctrl Pts',(-27.34981401959,22.5344663830884,-74.7269635750619));
#54770=CARTESIAN_POINT('Ctrl Pts',(-27.3205268577506,22.424917367907,-74.7212459852618));
#54771=CARTESIAN_POINT('Ctrl Pts',(-27.2864750423102,22.3165512540446,-74.7155283954617));
#54772=CARTESIAN_POINT('Ctrl Pts',(-27.2477829838819,22.2098206777215,-74.7098108056617));
#54773=CARTESIAN_POINT('Ctrl Pts',(-27.2091014823529,22.1031192222049,-74.7040947758721));
#54774=CARTESIAN_POINT('Ctrl Pts',(-27.1657823998924,21.9980528251032,-74.6983787460826));
#54775=CARTESIAN_POINT('Ctrl Pts',(-27.1179996559044,21.895057842937,-74.6926627162931));
#54776=CARTESIAN_POINT('Ctrl Pts',(-27.0702172636805,21.7920636189931,-74.6869467285835));
#54777=CARTESIAN_POINT('Ctrl Pts',(-27.0179714584404,21.6911411725022,-74.6812307408739));
#54778=CARTESIAN_POINT('Ctrl Pts',(-26.9614834250078,21.5927048841252,-74.6755147531643));
#54779=CARTESIAN_POINT('Ctrl Pts',(-26.9049808073633,21.4942431812382,-74.6697972896877));
#54780=CARTESIAN_POINT('Ctrl Pts',(-26.8442340028997,21.3982692864339,-74.6640798262111));
#54781=CARTESIAN_POINT('Ctrl Pts',(-26.7795085478587,21.3051702209391,-74.6583623627345));
#54782=CARTESIAN_POINT('Ctrl Pts',(-26.7147125334941,21.2119696651252,-74.652638666465));
#54783=CARTESIAN_POINT('Ctrl Pts',(-26.6459294636619,21.1216505464843,-74.6469149701956));
#54784=CARTESIAN_POINT('Ctrl Pts',(-26.5734662165351,21.0345681286359,-74.6411912739261));
#54785=CARTESIAN_POINT('Ctrl Pts',(-26.5009559978528,20.9474292629083,-74.6354638674873));
#54786=CARTESIAN_POINT('Ctrl Pts',(-26.424761149098,20.8635315891097,-74.6297364610485));
#54787=CARTESIAN_POINT('Ctrl Pts',(-26.3452251776108,20.7831932788812,-74.6240090546097));
#54788=CARTESIAN_POINT('Ctrl Pts',(-26.2655711448374,20.7027357163942,-74.6182731465463));
#54789=CARTESIAN_POINT('Ctrl Pts',(-26.1825664154429,20.6258483459862,-74.6125372384829));
#54790=CARTESIAN_POINT('Ctrl Pts',(-26.0965871078452,20.5528087496863,-74.6068013304195));
#54791=CARTESIAN_POINT('Ctrl Pts',(-26.0737271121074,20.5333891369124,-74.6052762793631));
#54792=CARTESIAN_POINT('Ctrl Pts',(-26.0506569937147,20.5142412863503,-74.6037512283067));
#54793=CARTESIAN_POINT('Ctrl Pts',(-26.0273841403122,20.4953698836068,-74.6022261772503));
#54794=CARTESIAN_POINT('Ctrl Pts',(-25.9376229399062,20.4225846632343,-74.5963441991732));
#54795=CARTESIAN_POINT('Ctrl Pts',(-25.8445036587257,20.3536394154685,-74.5904622210961));
#54796=CARTESIAN_POINT('Ctrl Pts',(-25.7483883828409,20.2888589982635,-74.5845802430191));
#54797=CARTESIAN_POINT('Ctrl Pts',(-25.6523972122015,20.2241622263428,-74.5787058598256));
#54798=CARTESIAN_POINT('Ctrl Pts',(-25.5534180788839,20.1636198179255,-74.5728314766321));
#54799=CARTESIAN_POINT('Ctrl Pts',(-25.4518464541428,20.1075167657507,-74.5669570934387));
#54800=CARTESIAN_POINT('Ctrl Pts',(-25.3503790679149,20.0514712896829,-74.5610887388676));
#54801=CARTESIAN_POINT('Ctrl Pts',(-25.2463248410248,19.9998563051262,-74.5552203842965));
#54802=CARTESIAN_POINT('Ctrl Pts',(-25.1401080253617,19.952913444361,-74.5493520297255));
#54803=CARTESIAN_POINT('Ctrl Pts',(-25.0299904827973,19.9042466448892,-74.543268164565));
#54804=CARTESIAN_POINT('Ctrl Pts',(-24.9175488362501,19.8606019713076,-74.5371842994046));
#54805=CARTESIAN_POINT('Ctrl Pts',(-24.8032839381334,19.8221965645074,-74.5311004342442));
#54806=CARTESIAN_POINT('Ctrl Pts',(-24.6931952093274,19.7851948038303,-74.5252389230297));
#54807=CARTESIAN_POINT('Ctrl Pts',(-24.5814145914695,19.753056191361,-74.5193774118151));
#54808=CARTESIAN_POINT('Ctrl Pts',(-24.4684094216106,19.7259255418175,-74.5135159006006));
#54809=CARTESIAN_POINT('Ctrl Pts',(-24.3554221781225,19.6987991960956,-74.5076553192163));
#54810=CARTESIAN_POINT('Ctrl Pts',(-24.2412111692231,19.6766793296322,-74.501794737832));
#54811=CARTESIAN_POINT('Ctrl Pts',(-24.1262566493561,19.6596602559042,-74.4959341564477));
#54812=CARTESIAN_POINT('Ctrl Pts',(-24.0112927871526,19.6426397990387,-74.4900730987749));
#54813=CARTESIAN_POINT('Ctrl Pts',(-23.895585701244,19.6307210192758,-74.484212041102));
#54814=CARTESIAN_POINT('Ctrl Pts',(-23.7796228533173,19.6239466017445,-74.4783509834292));
#54815=CARTESIAN_POINT('Ctrl Pts',(-23.663622761514,19.6171700084682,-74.4724880433559));
#54816=CARTESIAN_POINT('Ctrl Pts',(-23.5473671552413,19.6155410869641,-74.4666251032827));
#54817=CARTESIAN_POINT('Ctrl Pts',(-23.431344902167,19.6190504285659,-74.4607621632094));
#54818=CARTESIAN_POINT('Ctrl Pts',(-23.3151936817199,19.6225636710622,-74.4548927060418));
#54819=CARTESIAN_POINT('Ctrl Pts',(-23.1992767440886,19.631226564613,-74.4490232488741));
#54820=CARTESIAN_POINT('Ctrl Pts',(-23.0840793457134,19.6449776936485,-74.4431537917065));
#54821=CARTESIAN_POINT('Ctrl Pts',(-22.9688058692284,19.6587379041384,-74.4372804582603));
#54822=CARTESIAN_POINT('Ctrl Pts',(-22.8542532837516,19.6775929753553,-74.431407124814));
#54823=CARTESIAN_POINT('Ctrl Pts',(-22.7408964607948,19.7014304066151,-74.4255337913678));
#54824=CARTESIAN_POINT('Ctrl Pts',(-22.6273762254666,19.7253022013219,-74.4196519910704));
#54825=CARTESIAN_POINT('Ctrl Pts',(-22.515055590567,19.7541705892566,-74.4137701907731));
#54826=CARTESIAN_POINT('Ctrl Pts',(-22.4043941737707,19.7878732813292,-74.4078883904757));
#54827=CARTESIAN_POINT('Ctrl Pts',(-22.375864780954,19.7965621032236,-74.406372015609));
#54828=CARTESIAN_POINT('Ctrl Pts',(-22.3474455617636,19.8055719888764,-74.4048556407421));
#54829=CARTESIAN_POINT('Ctrl Pts',(-22.319144157869,19.8148996471735,-74.4033392658754));
#54830=CARTESIAN_POINT('Ctrl Pts',(-22.2093479792547,19.8510865882965,-74.3974564423116));
#54831=CARTESIAN_POINT('Ctrl Pts',(-22.1009722265775,19.8921767568183,-74.3915736187478));
#54832=CARTESIAN_POINT('Ctrl Pts',(-21.9944858986412,19.9380400263896,-74.385690795184));
#54833=CARTESIAN_POINT('Ctrl Pts',(-21.8881338225866,19.9838454741695,-74.3798153883482));
#54834=CARTESIAN_POINT('Ctrl Pts',(-21.7836668084796,20.0344118933758,-74.3739399815124));
#54835=CARTESIAN_POINT('Ctrl Pts',(-21.6815382297402,20.0895595580728,-74.3680645746766));
#54836=CARTESIAN_POINT('Ctrl Pts',(-21.5795113788949,20.1446522914679,-74.3621950201965));
#54837=CARTESIAN_POINT('Ctrl Pts',(-21.4798186900967,20.2043169983498,-74.3563254657164));
#54838=CARTESIAN_POINT('Ctrl Pts',(-21.3828924895577,20.2683263521846,-74.3504559112363));
#54839=CARTESIAN_POINT('Ctrl Pts',(-21.2824336297223,20.334668648378,-74.3443724297056));
#54840=CARTESIAN_POINT('Ctrl Pts',(-21.184947175876,20.4056781465189,-74.3382889481749));
#54841=CARTESIAN_POINT('Ctrl Pts',(-21.0908856904151,20.481050071768,-74.3322054666443));
#54842=CARTESIAN_POINT('Ctrl Pts',(-21.0002309680286,20.5536921412156,-74.326342319506));
#54843=CARTESIAN_POINT('Ctrl Pts',(-20.9127577730638,20.6303858405778,-74.3204791723677));
#54844=CARTESIAN_POINT('Ctrl Pts',(-20.8288400685972,20.710815403371,-74.3146160252294));
#54845=CARTESIAN_POINT('Ctrl Pts',(-20.7449333931878,20.7912343955432,-74.3087536486673));
#54846=CARTESIAN_POINT('Ctrl Pts',(-20.6645815762154,20.8753879900511,-74.3028912721052));
#54847=CARTESIAN_POINT('Ctrl Pts',(-20.5881229799605,20.9629223404071,-74.2970288955431));
#54848=CARTESIAN_POINT('Ctrl Pts',(-20.511656108692,21.050466164491,-74.2911658845036));
#54849=CARTESIAN_POINT('Ctrl Pts',(-20.4390835667527,21.1413911618974,-74.2853028734642));
#54850=CARTESIAN_POINT('Ctrl Pts',(-20.3707040935097,21.2353096103161,-74.2794398624247));
#54851=CARTESIAN_POINT('Ctrl Pts',(-20.3023008322258,21.3292607313452,-74.2735748117448));
#54852=CARTESIAN_POINT('Ctrl Pts',(-20.2380937826937,21.4262070417607,-74.2677097610648));
#54853=CARTESIAN_POINT('Ctrl Pts',(-20.1783385474773,21.5257315801991,-74.2618447103848));
#54854=CARTESIAN_POINT('Ctrl Pts',(-20.1185146289072,21.6253705132851,-74.2559729183482));
#54855=CARTESIAN_POINT('Ctrl Pts',(-20.0631529501736,21.7275932363411,-74.2501011263116));
#54856=CARTESIAN_POINT('Ctrl Pts',(-20.0124633577918,21.8319578069689,-74.244229334275));
#54857=CARTESIAN_POINT('Ctrl Pts',(-19.9617391481416,21.9363936509325,-74.2383535322357));
#54858=CARTESIAN_POINT('Ctrl Pts',(-19.9156935415742,22.0429738783499,-74.2324777301965));
#54859=CARTESIAN_POINT('Ctrl Pts',(-19.8744877478804,22.1512377876424,-74.2266019281572));
#54860=CARTESIAN_POINT('Ctrl Pts',(-19.8332213284705,22.2596609846572,-74.2207174811029));
#54861=CARTESIAN_POINT('Ctrl Pts',(-19.7968090627029,22.3697724182824,-74.2148330340487));
#54862=CARTESIAN_POINT('Ctrl Pts',(-19.7653619995541,22.4810974167946,-74.2089485869944));
#54863=CARTESIAN_POINT('Ctrl Pts',(-19.7573525635011,22.5094514304097,-74.2074498428297));
#54864=CARTESIAN_POINT('Ctrl Pts',(-19.7496649597729,22.5378841250592,-74.2059510986651));
#54865=CARTESIAN_POINT('Ctrl Pts',(-19.7423004883812,22.5663875837321,-74.2044523545005));
#54866=CARTESIAN_POINT('Ctrl Pts',(-19.7134867755638,22.6779082114623,-74.1985884734901));
#54867=CARTESIAN_POINT('Ctrl Pts',(-19.6895266558515,22.7908876659337,-74.1927245924796));
#54868=CARTESIAN_POINT('Ctrl Pts',(-19.6705664942649,22.9048648567452,-74.1868607114692));
#54869=CARTESIAN_POINT('Ctrl Pts',(-19.6516312761111,23.0186921025053,-74.1810045448088));
#54870=CARTESIAN_POINT('Ctrl Pts',(-19.6376830036379,23.1335140693503,-74.1751483781483));
#54871=CARTESIAN_POINT('Ctrl Pts',(-19.6288179866241,23.2488556028265,-74.1692922114879));
#54872=CARTESIAN_POINT('Ctrl Pts',(-19.6199622419566,23.3640764950626,-74.1634421700729));
#54873=CARTESIAN_POINT('Ctrl Pts',(-19.6161792097235,23.4798154621531,-74.1575921286579));
#54874=CARTESIAN_POINT('Ctrl Pts',(-19.6175138410972,23.5955889572455,-74.151742087243));
#54875=CARTESIAN_POINT('Ctrl Pts',(-19.6189033749591,23.7161250055534,-74.1456513937381));
#54876=CARTESIAN_POINT('Ctrl Pts',(-19.6258407228482,23.8366980322504,-74.1395607002332));
#54877=CARTESIAN_POINT('Ctrl Pts',(-19.6383166657902,23.9567581049082,-74.1334700067283));
#54878=CARTESIAN_POINT('Ctrl Pts',(-19.650285395133,24.0719370954819,-74.1276269323885));
#54879=CARTESIAN_POINT('Ctrl Pts',(-19.6673511371457,24.1866435710266,-74.1217838580486));
#54880=CARTESIAN_POINT('Ctrl Pts',(-19.6894526486738,24.3003946937339,-74.1159407837087));
#54881=CARTESIAN_POINT('Ctrl Pts',(-19.7115505912792,24.4141274480615,-74.1100986529007));
#54882=CARTESIAN_POINT('Ctrl Pts',(-19.7386826076022,24.5269047492561,-74.1042565220927));
#54883=CARTESIAN_POINT('Ctrl Pts',(-19.7707361355208,24.6382529044222,-74.0984143912847));
#54884=CARTESIAN_POINT('Ctrl Pts',(-19.8027923108917,24.7496102563587,-74.0925717779475));
#54885=CARTESIAN_POINT('Ctrl Pts',(-19.8397706910818,24.8595378290581,-74.0867291646104));
#54886=CARTESIAN_POINT('Ctrl Pts',(-19.8815087436497,24.9675767774775,-74.0808865512732));
#54887=CARTESIAN_POINT('Ctrl Pts',(-19.9232604307852,25.0756510189747,-74.0750420293298));
#54888=CARTESIAN_POINT('Ctrl Pts',(-19.9697747323456,25.1818350228425,-74.0691975073864));
#54889=CARTESIAN_POINT('Ctrl Pts',(-20.0208411431113,25.2856903007142,-74.063352985443));
#54890=CARTESIAN_POINT('Ctrl Pts',(-20.0719656566824,25.3896637439887,-74.0575018136662));
#54891=CARTESIAN_POINT('Ctrl Pts',(-20.1276524339694,25.4913028004289,-74.0516506418895));
#54892=CARTESIAN_POINT('Ctrl Pts',(-20.187645168696,25.5901938843587,-74.0457994701128));
#54893=CARTESIAN_POINT('Ctrl Pts',(-20.2476782100473,25.6891514090969,-74.0399443671769));
#54894=CARTESIAN_POINT('Ctrl Pts',(-20.3120227388763,25.7853569415034,-74.0340892642411));
#54895=CARTESIAN_POINT('Ctrl Pts',(-20.3803803378345,25.8784276270414,-74.0282341613053));
#54896=CARTESIAN_POINT('Ctrl Pts',(-20.4488393836399,25.9716364351548,-74.0223703690395));
#54897=CARTESIAN_POINT('Ctrl Pts',(-20.5213231265793,26.0617007896389,-74.0165065767737));
#54898=CARTESIAN_POINT('Ctrl Pts',(-20.5974942498583,26.1482724563772,-74.0106427845079));
#54899=CARTESIAN_POINT('Ctrl Pts',(-20.6194792713164,26.1732593525784,-74.0089503373805));
#54900=CARTESIAN_POINT('Ctrl Pts',(-20.6417712484578,26.1979555352059,-74.007257890253));
#54901=CARTESIAN_POINT('Ctrl Pts',(-20.6643615458576,26.2223532442174,-74.0055654431255));
#54902=CARTESIAN_POINT('Ctrl Pts',(-20.7427683912889,26.3070332891714,-73.99969126458));
#54903=CARTESIAN_POINT('Ctrl Pts',(-20.8250362932512,26.3884006391815,-73.9938170860344));
#54904=CARTESIAN_POINT('Ctrl Pts',(-20.9108542445527,26.4660827191082,-73.9879429074889));
#54905=CARTESIAN_POINT('Ctrl Pts',(-20.9965611353252,26.5436642674705,-73.9820763309586));
#54906=CARTESIAN_POINT('Ctrl Pts',(-21.0858086355093,26.6175697555757,-73.9762097544284));
#54907=CARTESIAN_POINT('Ctrl Pts',(-21.1782469736425,26.687461264401,-73.9703431778981));
#54908=CARTESIAN_POINT('Ctrl Pts',(-21.2705903648361,26.7572809849944,-73.9644826271521));
#54909=CARTESIAN_POINT('Ctrl Pts',(-21.3661177473683,26.8230946794785,-73.9586220764062));
#54910=CARTESIAN_POINT('Ctrl Pts',(-21.4644446524362,26.884603216734,-73.9527615256602));
#54911=CARTESIAN_POINT('Ctrl Pts',(-21.5665673687757,26.9484862292041,-73.9466747342473));
#54912=CARTESIAN_POINT('Ctrl Pts',(-21.6717097729922,27.0077246879211,-73.9405879428344));
#54913=CARTESIAN_POINT('Ctrl Pts',(-21.7794056283828,27.0620313181545,-73.9345011514215));
#54914=CARTESIAN_POINT('Ctrl Pts',(-21.8829785022079,27.1142588968355,-73.9286473840995));
#54915=CARTESIAN_POINT('Ctrl Pts',(-21.9889125080763,27.1619251180764,-73.9227936167774));
#54916=CARTESIAN_POINT('Ctrl Pts',(-22.096766657896,27.204820606675,-73.9169398494553));
#54917=CARTESIAN_POINT('Ctrl Pts',(-22.2046043441469,27.2477095474234,-73.9110869756909));
#54918=CARTESIAN_POINT('Ctrl Pts',(-22.3143612078228,27.2858290509121,-73.9052341019265));
#54919=CARTESIAN_POINT('Ctrl Pts',(-22.4255762965451,27.3190178953234,-73.8993812281621));
#54920=CARTESIAN_POINT('Ctrl Pts',(-22.5368012936864,27.3522096966084,-73.8935278329511));
#54921=CARTESIAN_POINT('Ctrl Pts',(-22.6494843782854,27.3804698474238,-73.8876744377401));
#54922=CARTESIAN_POINT('Ctrl Pts',(-22.7631501424009,27.4036872111417,-73.8818210425292));
#54923=CARTESIAN_POINT('Ctrl Pts',(-22.8768535106594,27.4269122558802,-73.8759657108344));
#54924=CARTESIAN_POINT('Ctrl Pts',(-22.9915398003756,27.4450911135209,-73.8701103791396));
#54925=CARTESIAN_POINT('Ctrl Pts',(-23.1067248418525,27.4581640184533,-73.8642550474449));
#54926=CARTESIAN_POINT('Ctrl Pts',(-23.2220404474327,27.4712517417344,-73.8583930786371));
#54927=CARTESIAN_POINT('Ctrl Pts',(-23.3378555224973,27.4792219136071,-73.8525311098294));
#54928=CARTESIAN_POINT('Ctrl Pts',(-23.4536821185467,27.4820667637383,-73.8466691410216));
#54929=CARTESIAN_POINT('Ctrl Pts',(-23.5695865123549,27.4849135246825,-73.8408032348796));
#54930=CARTESIAN_POINT('Ctrl Pts',(-23.6855020305534,27.4826281170552,-73.8349373287375));
#54931=CARTESIAN_POINT('Ctrl Pts',(-23.8009438151018,27.4752548094545,-73.8290714225954));
#54932=CARTESIAN_POINT('Ctrl Pts',(-23.9165551367192,27.4678706734613,-73.8231969018209));
#54933=CARTESIAN_POINT('Ctrl Pts',(-24.0316909270041,27.4553837689823,-73.8173223810464));
#54934=CARTESIAN_POINT('Ctrl Pts',(-24.1458744202636,27.4378898046219,-73.811447860272));
#54935=CARTESIAN_POINT('Ctrl Pts',(-24.1767750169227,27.4331555481963,-73.8098580840982));
#54936=CARTESIAN_POINT('Ctrl Pts',(-24.2076059476972,27.4280548775577,-73.8082683079245));
#54937=CARTESIAN_POINT('Ctrl Pts',(-24.2383579509695,27.422590318092,-73.8066785317508));
#54938=CARTESIAN_POINT('Ctrl Pts',(-24.3519742737502,27.4024009617558,-73.8008049461731));
#54939=CARTESIAN_POINT('Ctrl Pts',(-24.4648906384944,27.3771733823538,-73.7949313605954));
#54940=CARTESIAN_POINT('Ctrl Pts',(-24.5766255530572,27.346967878019,-73.7890577750178));
#54941=CARTESIAN_POINT('Ctrl Pts',(-24.6882161795882,27.3168013793324,-73.7831917742502));
#54942=CARTESIAN_POINT('Ctrl Pts',(-24.7986279947573,27.2816698461074,-73.7773257734825));
#54943=CARTESIAN_POINT('Ctrl Pts',(-24.9073877158074,27.2416849219788,-73.7714597727149));
#54944=CARTESIAN_POINT('Ctrl Pts',(-25.0160360453782,27.201740950326,-73.765599779893));
#54945=CARTESIAN_POINT('Ctrl Pts',(-25.123035261007,27.1569536168588,-73.7597397870712));
#54946=CARTESIAN_POINT('Ctrl Pts',(-25.2279259647884,27.1074847214578,-73.7538797942493));
#54947=CARTESIAN_POINT('Ctrl Pts',(-25.3368801040218,27.0560994153921,-73.7477927870045));
#54948=CARTESIAN_POINT('Ctrl Pts',(-25.4435586228252,26.999662605872,-73.7417057797598));
#54949=CARTESIAN_POINT('Ctrl Pts',(-25.5474677321391,26.9384113891139,-73.7356187725151));
#54950=CARTESIAN_POINT('Ctrl Pts',(-25.6473865916651,26.8795123015993,-73.7297655145492));
#54951=CARTESIAN_POINT('Ctrl Pts',(-25.7447444286019,26.8161619765703,-73.7239122565833));
#54952=CARTESIAN_POINT('Ctrl Pts',(-25.8391268258036,26.7486182809113,-73.7180589986174));
#54953=CARTESIAN_POINT('Ctrl Pts',(-25.9334951195196,26.6810846782524,-73.7122066152992));
#54954=CARTESIAN_POINT('Ctrl Pts',(-26.0248885216434,26.6093591912674,-73.7063542319809));
#54955=CARTESIAN_POINT('Ctrl Pts',(-26.1129223459199,26.5337425054089,-73.7005018486627));
#54956=CARTESIAN_POINT('Ctrl Pts',(-26.2009643078742,26.4581188296892,-73.6946489243613));
#54957=CARTESIAN_POINT('Ctrl Pts',(-26.2856457611703,26.3786035092642,-73.68879600006));
#54958=CARTESIAN_POINT('Ctrl Pts',(-26.366616353408,26.2955364557614,-73.6829430757587));
#54959=CARTESIAN_POINT('Ctrl Pts',(-26.4476140145222,26.2124416325245,-73.6770881947953));
#54960=CARTESIAN_POINT('Ctrl Pts',(-26.5248980595177,26.1257930108825,-73.6712333138319));
#54961=CARTESIAN_POINT('Ctrl Pts',(-26.5981566290412,26.0359656312644,-73.6653784328685));
#54962=CARTESIAN_POINT('Ctrl Pts',(-26.6714986507999,25.9460359251111,-73.6595168823386));
#54963=CARTESIAN_POINT('Ctrl Pts',(-26.7408057830521,25.852920553796,-73.6536553318087));
#54964=CARTESIAN_POINT('Ctrl Pts',(-26.8058078761404,25.7570258320692,-73.6477937812787));
#54965=CARTESIAN_POINT('Ctrl Pts',(-26.8708538366292,25.6610663947006,-73.6419282750149));
#54966=CARTESIAN_POINT('Ctrl Pts',(-26.9315887569188,25.5623242231031,-73.636062768751));
#54967=CARTESIAN_POINT('Ctrl Pts',(-26.9877879478463,25.4612311455724,-73.6301972624872));
#54968=CARTESIAN_POINT('Ctrl Pts',(-27.0440699684829,25.3599890710533,-73.6243231112915));
#54969=CARTESIAN_POINT('Ctrl Pts',(-27.0958027338074,25.25638954356,-73.6184489600958));
#54970=CARTESIAN_POINT('Ctrl Pts',(-27.14280921265,25.1508853734538,-73.6125748089));
#54971=CARTESIAN_POINT('Ctrl Pts',(-27.155567983672,25.1222488199109,-73.6109804127253));
#54972=CARTESIAN_POINT('Ctrl Pts',(-27.1679788427514,25.0934720372478,-73.6093860165506));
#54973=CARTESIAN_POINT('Ctrl Pts',(-27.1800388861824,25.0645642633964,-73.6077916203759));
#54974=CARTESIAN_POINT('Ctrl Pts',(-27.2296008949614,24.945764745833,-73.6012392826782));
#54975=CARTESIAN_POINT('Ctrl Pts',(-27.2733751995325,24.8244139971785,-73.5946869449805));
#54976=CARTESIAN_POINT('Ctrl Pts',(-27.3111208139817,24.7010604058781,-73.5881346072828));
#54977=CARTESIAN_POINT('Ctrl Pts',(-27.3487184499471,24.5781904118824,-73.5816079574699));
#54978=CARTESIAN_POINT('Ctrl Pts',(-27.3803344475293,24.4533334638435,-73.5750813076571));
#54979=CARTESIAN_POINT('Ctrl Pts',(-27.4057768105741,24.3270546525509,-73.5685546578443));
#54980=CARTESIAN_POINT('Ctrl Pts',(-27.4313693794316,24.200030320434,-73.5619894762041));
#54981=CARTESIAN_POINT('Ctrl Pts',(-27.4507150012671,24.0715674845368,-73.555424294564));
#54982=CARTESIAN_POINT('Ctrl Pts',(-27.4636676401974,23.9422617006414,-73.5488591129239));
#54983=CARTESIAN_POINT('Ctrl Pts',(-27.4766202791278,23.812955916746,-73.5422939312838));
#54984=CARTESIAN_POINT('Ctrl Pts',(-27.4831797858945,23.6828074206673,-73.5357287496436));
#54985=CARTESIAN_POINT('Ctrl Pts',(-27.4832519295814,23.5524288172932,-73.5291635680035));
#54986=CARTESIAN_POINT('',(-27.4799905867943,23.5470322484969,-72.2791635220347));
#54987=CARTESIAN_POINT('Ctrl Pts',(-27.4778725016352,23.55242492899,-73.5291635220347));
#54988=CARTESIAN_POINT('Ctrl Pts',(-27.4739703607174,22.7574340764279,-73.4890772510234));
#54989=CARTESIAN_POINT('Ctrl Pts',(-26.8529990368603,20.6420195649947,-73.3826953428873));
#54990=CARTESIAN_POINT('Ctrl Pts',(-23.3948704418965,18.9009230350336,-73.210017797626));
#54991=CARTESIAN_POINT('Ctrl Pts',(-19.554684473212,21.167768508944,-73.0111308862512));
#54992=CARTESIAN_POINT('Ctrl Pts',(-19.3860646478423,25.6239837848511,-72.8122439748762));
#54993=CARTESIAN_POINT('Ctrl Pts',(-23.0439921451409,28.174579327054,-72.6133570635014));
#54994=CARTESIAN_POINT('Ctrl Pts',(-26.7277621119337,26.656849026205,-72.4356635792209));
#54995=CARTESIAN_POINT('Ctrl Pts',(-27.4731413038454,24.4402793233453,-72.3242657320653));
#54996=CARTESIAN_POINT('Ctrl Pts',(-27.4799905867943,23.5470322484969,-72.2791635220347));
#54997=CARTESIAN_POINT('',(-27.4856295271234,23.5494159766936,-71.0291638765219));
#54998=CARTESIAN_POINT('Ctrl Pts',(-27.4799905867943,23.5470322484969,-72.2791635220347));
#54999=CARTESIAN_POINT('Ctrl Pts',(-27.4832090494534,23.1272974562284,-72.2579700949403));
#55000=CARTESIAN_POINT('Ctrl Pts',(-27.2276593103525,21.398397011866,-72.1704810307208));
#55001=CARTESIAN_POINT('Ctrl Pts',(-24.7078912105456,19.0446320962057,-72.0166963293769));
#55002=CARTESIAN_POINT('Ctrl Pts',(-20.3853508355522,20.14083173501,-71.8178094180018));
#55003=CARTESIAN_POINT('Ctrl Pts',(-18.9710862915074,24.3700015369503,-71.618922506627));
#55004=CARTESIAN_POINT('Ctrl Pts',(-21.7646875315776,27.8458907001526,-71.420035595252));
#55005=CARTESIAN_POINT('Ctrl Pts',(-26.1477706968028,27.3799070216123,-71.2234495793812));
#55006=CARTESIAN_POINT('Ctrl Pts',(-27.4858620735673,24.8089282503745,-71.0931592006353));
#55007=CARTESIAN_POINT('Ctrl Pts',(-27.4895355474849,23.5494266036718,-71.0291644590143));
#55008=CARTESIAN_POINT('',(-27.4832508538687,23.5538854055544,-69.7791635439327));
#55009=CARTESIAN_POINT('Ctrl Pts',(-27.483252441345,23.5494095094363,-71.0291635220347));
#55010=CARTESIAN_POINT('Ctrl Pts',(-27.4832427515645,23.5042032228065,-71.0268629388572));
#55011=CARTESIAN_POINT('Ctrl Pts',(-27.4824536810313,23.4590061945149,-71.0245623556797));
#55012=CARTESIAN_POINT('Ctrl Pts',(-27.4808860205748,23.41383634464,-71.0222617725022));
#55013=CARTESIAN_POINT('Ctrl Pts',(-27.4768845272569,23.2985391502213,-71.0163894752369));
#55014=CARTESIAN_POINT('Ctrl Pts',(-27.4677990137816,23.1832250148259,-71.0105171779717));
#55015=CARTESIAN_POINT('Ctrl Pts',(-27.4536211817208,23.0683789154942,-71.0046448807064));
#55016=CARTESIAN_POINT('Ctrl Pts',(-27.4394617229954,22.9536816475135,-70.9987801934683));
#55017=CARTESIAN_POINT('Ctrl Pts',(-27.420223119379,22.8394516158931,-70.9929155062302));
#55018=CARTESIAN_POINT('Ctrl Pts',(-27.3959490620305,22.7261729259768,-70.9870508189921));
#55019=CARTESIAN_POINT('Ctrl Pts',(-27.3716999690168,22.6130107360384,-70.9811921632145));
#55020=CARTESIAN_POINT('Ctrl Pts',(-27.3424258089596,22.5007983435031,-70.9753335074368));
#55021=CARTESIAN_POINT('Ctrl Pts',(-27.3082218870988,22.3900131926612,-70.9694748516592));
#55022=CARTESIAN_POINT('Ctrl Pts',(-27.2726819324168,22.2749006843241,-70.9633873520537));
#55023=CARTESIAN_POINT('Ctrl Pts',(-27.2318192995848,22.161329640374,-70.9572998524482));
#55024=CARTESIAN_POINT('Ctrl Pts',(-27.1857991426444,22.0498226467585,-70.9512123528427));
#55025=CARTESIAN_POINT('Ctrl Pts',(-27.1415602906898,21.9426317610592,-70.945360482451));
#55026=CARTESIAN_POINT('Ctrl Pts',(-27.0925559282324,21.837348527908,-70.9395086120592));
#55027=CARTESIAN_POINT('Ctrl Pts',(-27.0389828294276,21.7344194144511,-70.9336567416675));
#55028=CARTESIAN_POINT('Ctrl Pts',(-26.9854178876001,21.6315059728603,-70.9278057622747));
#55029=CARTESIAN_POINT('Ctrl Pts',(-26.9272857833643,21.5309463048658,-70.921954782882));
#55030=CARTESIAN_POINT('Ctrl Pts',(-26.8648298748244,21.4331634838721,-70.9161038034892));
#55031=CARTESIAN_POINT('Ctrl Pts',(-26.8023683508848,21.3353718712423,-70.9102522980359));
#55032=CARTESIAN_POINT('Ctrl Pts',(-26.7355824723696,21.2403579503292,-70.9044007925826));
#55033=CARTESIAN_POINT('Ctrl Pts',(-26.6647592727034,21.1485163346467,-70.8985492871293));
#55034=CARTESIAN_POINT('Ctrl Pts',(-26.5939125541853,21.0566442203512,-70.8926958385177));
#55035=CARTESIAN_POINT('Ctrl Pts',(-26.5190261009088,20.9679468331937,-70.8868423899061));
#55036=CARTESIAN_POINT('Ctrl Pts',(-26.4404271499071,20.8827856291371,-70.8809889412945));
#55037=CARTESIAN_POINT('Ctrl Pts',(-26.3617388148394,20.7975275783083,-70.8751288360414));
#55038=CARTESIAN_POINT('Ctrl Pts',(-26.2793298357643,20.7158140411441,-70.8692687307883));
#55039=CARTESIAN_POINT('Ctrl Pts',(-26.1935642885217,20.6379695859251,-70.8634086255352));
#55040=CARTESIAN_POINT('Ctrl Pts',(-26.1077409835509,20.5600727073376,-70.857544573868));
#55041=CARTESIAN_POINT('Ctrl Pts',(-26.0185569267443,20.4860503623003,-70.8516805222007));
#55042=CARTESIAN_POINT('Ctrl Pts',(-25.9264078561718,20.4161857050364,-70.8458164705335));
#55043=CARTESIAN_POINT('Ctrl Pts',(-25.8341229763041,20.3462180812444,-70.8399437764272));
#55044=CARTESIAN_POINT('Ctrl Pts',(-25.738864700173,20.2804206087893,-70.834071082321));
#55045=CARTESIAN_POINT('Ctrl Pts',(-25.6410562499928,20.2190322130198,-70.8281983882147));
#55046=CARTESIAN_POINT('Ctrl Pts',(-25.614277983195,20.2022251289982,-70.8265905458523));
#55047=CARTESIAN_POINT('Ctrl Pts',(-25.5873086936766,20.1857482644168,-70.8249827034899));
#55048=CARTESIAN_POINT('Ctrl Pts',(-25.5601573454409,20.1696059012879,-70.8233748611275));
#55049=CARTESIAN_POINT('Ctrl Pts',(-25.4609929105405,20.1106494066143,-70.8175025641833));
#55050=CARTESIAN_POINT('Ctrl Pts',(-25.359066094642,20.0559610254743,-70.8116302672392));
#55051=CARTESIAN_POINT('Ctrl Pts',(-25.2547804313492,20.0058098901358,-70.8057579702949));
#55052=CARTESIAN_POINT('Ctrl Pts',(-25.1506299139877,19.9557237466827,-70.7998932833808));
#55053=CARTESIAN_POINT('Ctrl Pts',(-25.0441269973708,19.9101633335037,-70.7940285964668));
#55054=CARTESIAN_POINT('Ctrl Pts',(-24.9357025843097,19.8693535719688,-70.7881639095527));
#55055=CARTESIAN_POINT('Ctrl Pts',(-24.827389678963,19.8285857807163,-70.7823052541015));
#55056=CARTESIAN_POINT('Ctrl Pts',(-24.7171595923729,19.7925590678489,-70.7764465986504));
#55057=CARTESIAN_POINT('Ctrl Pts',(-24.6054655228979,19.7614513303648,-70.7705879431993));
#55058=CARTESIAN_POINT('Ctrl Pts',(-24.4894085840485,19.7291284970765,-70.7645004434723));
#55059=CARTESIAN_POINT('Ctrl Pts',(-24.3717713715992,19.7021169492531,-70.7584129437454));
#55060=CARTESIAN_POINT('Ctrl Pts',(-24.2530828186991,19.6805602199375,-70.7523254440185));
#55061=CARTESIAN_POINT('Ctrl Pts',(-24.1389883594895,19.6598378898266,-70.7464735739576));
#55062=CARTESIAN_POINT('Ctrl Pts',(-24.0239228798842,19.6441560301766,-70.7406217038967));
#55063=CARTESIAN_POINT('Ctrl Pts',(-23.9083683649091,19.633590426023,-70.7347698338358));
#55064=CARTESIAN_POINT('Ctrl Pts',(-23.7928314441503,19.6230264305778,-70.7289188547749));
#55065=CARTESIAN_POINT('Ctrl Pts',(-23.6768060476247,19.6175771793654,-70.7230678757139));
#55066=CARTESIAN_POINT('Ctrl Pts',(-23.5607796594119,19.6172666202546,-70.717216896653));
#55067=CARTESIAN_POINT('Ctrl Pts',(-23.4447428393001,19.6169560332216,-70.7113653915323));
#55068=CARTESIAN_POINT('Ctrl Pts',(-23.3287054407299,19.6217850578465,-70.7055138864115));
#55069=CARTESIAN_POINT('Ctrl Pts',(-23.2131546123612,19.6317255134409,-70.6996623812907));
#55070=CARTESIAN_POINT('Ctrl Pts',(-23.0975654120675,19.641669270045,-70.693808933012));
#55071=CARTESIAN_POINT('Ctrl Pts',(-22.9824635149095,19.6567277973703,-70.6879554847332));
#55072=CARTESIAN_POINT('Ctrl Pts',(-22.868329905299,19.6768211676953,-70.6821020364545));
#55073=CARTESIAN_POINT('Ctrl Pts',(-22.7540665009729,19.6969373885488,-70.6762419315331));
#55074=CARTESIAN_POINT('Ctrl Pts',(-22.6407739894265,19.7220998090305,-70.6703818266116));
#55075=CARTESIAN_POINT('Ctrl Pts',(-22.528922233783,19.7521775689573,-70.6645217216902));
#55076=CARTESIAN_POINT('Ctrl Pts',(-22.4169951529728,19.7822755843756,-70.6586576703544));
#55077=CARTESIAN_POINT('Ctrl Pts',(-22.3065111531423,19.8172954058531,-70.6527936190186));
#55078=CARTESIAN_POINT('Ctrl Pts',(-22.1979223698499,19.8570571491879,-70.6469295676827));
#55079=CARTESIAN_POINT('Ctrl Pts',(-22.0891735483504,19.8968774934013,-70.6410568739049));
#55080=CARTESIAN_POINT('Ctrl Pts',(-21.9823258981003,19.9414535488962,-70.6351841801271));
#55081=CARTESIAN_POINT('Ctrl Pts',(-21.8778092005089,19.9905584010175,-70.6293114863492));
#55082=CARTESIAN_POINT('Ctrl Pts',(-21.8491942732487,20.0040024898948,-70.6277036408169));
#55083=CARTESIAN_POINT('Ctrl Pts',(-21.8207539099472,20.01778578834,-70.6260957952846));
#55084=CARTESIAN_POINT('Ctrl Pts',(-21.7924965586072,20.0319030693643,-70.6244879497523));
#55085=CARTESIAN_POINT('Ctrl Pts',(-21.6892928905123,20.083463287012,-70.6186156528528));
#55086=CARTESIAN_POINT('Ctrl Pts',(-21.5881868738218,20.1396546383768,-70.6127433559532));
#55087=CARTESIAN_POINT('Ctrl Pts',(-21.4896230610458,20.2002831012821,-70.6068710590536));
#55088=CARTESIAN_POINT('Ctrl Pts',(-21.3911869791644,20.2608329945016,-70.6010063721857));
#55089=CARTESIAN_POINT('Ctrl Pts',(-21.2952868984824,20.3258083497012,-70.5951416853178));
#55090=CARTESIAN_POINT('Ctrl Pts',(-21.2023449703586,20.3949682206656,-70.5892769984499));
#55091=CARTESIAN_POINT('Ctrl Pts',(-21.1094986272077,20.4640569650188,-70.5834183430464));
#55092=CARTESIAN_POINT('Ctrl Pts',(-21.0196047150193,20.5373214199315,-70.577559687643));
#55093=CARTESIAN_POINT('Ctrl Pts',(-20.9330578744486,20.6144764629033,-70.5717010322395));
#55094=CARTESIAN_POINT('Ctrl Pts',(-20.8431304365711,20.6946452511344,-70.5656135324952));
#55095=CARTESIAN_POINT('Ctrl Pts',(-20.756817267376,20.7790145250746,-70.559526032751));
#55096=CARTESIAN_POINT('Ctrl Pts',(-20.6745250344264,20.8672168700866,-70.5534385330068));
#55097=CARTESIAN_POINT('Ctrl Pts',(-20.5954180988584,20.9520051541534,-70.5475866629969));
#55098=CARTESIAN_POINT('Ctrl Pts',(-20.520026917881,21.0403349619105,-70.5417347929872));
#55099=CARTESIAN_POINT('Ctrl Pts',(-20.4486757840577,21.1318417563046,-70.5358829229773));
#55100=CARTESIAN_POINT('Ctrl Pts',(-20.3773355141019,21.223334617946,-70.5300319439687));
#55101=CARTESIAN_POINT('Ctrl Pts',(-20.3100343223364,21.3180031785176,-70.5241809649599));
#55102=CARTESIAN_POINT('Ctrl Pts',(-20.2470558623188,21.4154502543328,-70.5183299859513));
#55103=CARTESIAN_POINT('Ctrl Pts',(-20.1840717399382,21.5129060915677,-70.5124784808839));
#55104=CARTESIAN_POINT('Ctrl Pts',(-20.1254113463097,21.613140593448,-70.5066269758165));
#55105=CARTESIAN_POINT('Ctrl Pts',(-20.0713142970534,21.715728680785,-70.5007754707491));
#55106=CARTESIAN_POINT('Ctrl Pts',(-20.0171992833495,21.8183508353835,-70.4949220225247));
#55107=CARTESIAN_POINT('Ctrl Pts',(-19.9676508199871,21.9233277640855,-70.4890685743004));
#55108=CARTESIAN_POINT('Ctrl Pts',(-19.9228616549023,22.030211602322,-70.4832151260761));
#55109=CARTESIAN_POINT('Ctrl Pts',(-19.8780215548136,22.1372169906856,-70.4773550212104));
#55110=CARTESIAN_POINT('Ctrl Pts',(-19.8379517157607,22.2461332354966,-70.4714949163448));
#55111=CARTESIAN_POINT('Ctrl Pts',(-19.8027960238171,22.3564942975573,-70.4656348114791));
#55112=CARTESIAN_POINT('Ctrl Pts',(-19.767616656717,22.4669296808805,-70.4597707601999));
#55113=CARTESIAN_POINT('Ctrl Pts',(-19.7373581339983,22.5788114208061,-70.4539067089207));
#55114=CARTESIAN_POINT('Ctrl Pts',(-19.7121135145048,22.6916618930725,-70.4480426576414));
#55115=CARTESIAN_POINT('Ctrl Pts',(-19.6868316894807,22.8046786844118,-70.442169963921));
#55116=CARTESIAN_POINT('Ctrl Pts',(-19.6665785877282,22.9186666520617,-70.4362972702006));
#55117=CARTESIAN_POINT('Ctrl Pts',(-19.6513956172167,23.0331415567276,-70.4304245764801));
#55118=CARTESIAN_POINT('Ctrl Pts',(-19.647238771979,23.0644828849565,-70.428816730446));
#55119=CARTESIAN_POINT('Ctrl Pts',(-19.6434616689011,23.0958607067755,-70.4272088844118));
#55120=CARTESIAN_POINT('Ctrl Pts',(-19.6400644769335,23.1272650893196,-70.4256010383776));
#55121=CARTESIAN_POINT('Ctrl Pts',(-19.6276569952297,23.2419625528554,-70.4197287413624));
#55122=CARTESIAN_POINT('Ctrl Pts',(-19.6202796337672,23.3573985511179,-70.4138564443473));
#55123=CARTESIAN_POINT('Ctrl Pts',(-19.6180094578943,23.4730941973888,-70.4079841473321));
#55124=CARTESIAN_POINT('Ctrl Pts',(-19.6157422239888,23.5886399113025,-70.4021194603469));
#55125=CARTESIAN_POINT('Ctrl Pts',(-19.6185690218743,23.7044441945922,-70.3962547733617));
#55126=CARTESIAN_POINT('Ctrl Pts',(-19.6265153301458,23.8200216425744,-70.3903900863765));
#55127=CARTESIAN_POINT('Ctrl Pts',(-19.6344534661374,23.9354802263973,-70.3845314308542));
#55128=CARTESIAN_POINT('Ctrl Pts',(-19.6475006117855,24.0507120290006,-70.3786727753319));
#55129=CARTESIAN_POINT('Ctrl Pts',(-19.6656302087334,24.1652309117649,-70.3728141198095));
#55130=CARTESIAN_POINT('Ctrl Pts',(-19.6844679634991,24.2842230016476,-70.3667266201092));
#55131=CARTESIAN_POINT('Ctrl Pts',(-19.7087933227104,24.4024448871687,-70.360639120409));
#55132=CARTESIAN_POINT('Ctrl Pts',(-19.7385169953152,24.5193558289259,-70.3545516207087));
#55133=CARTESIAN_POINT('Ctrl Pts',(-19.7670901502209,24.6317414850802,-70.3486997505768));
#55134=CARTESIAN_POINT('Ctrl Pts',(-19.8006513714833,24.7429153581334,-70.342847880445));
#55135=CARTESIAN_POINT('Ctrl Pts',(-19.8390692618257,24.8524075675668,-70.3369960103131));
#55136=CARTESIAN_POINT('Ctrl Pts',(-19.8774813026968,24.9618831058207,-70.3311450311815));
#55137=CARTESIAN_POINT('Ctrl Pts',(-19.9207484055142,25.0696770995997,-70.3252940520498));
#55138=CARTESIAN_POINT('Ctrl Pts',(-19.9686897397363,25.1753362117743,-70.3194430729181));
#55139=CARTESIAN_POINT('Ctrl Pts',(-20.0166353843474,25.2810048237237,-70.3135915677269));
#55140=CARTESIAN_POINT('Ctrl Pts',(-20.0692559249819,25.3845377960297,-70.3077400625357));
#55141=CARTESIAN_POINT('Ctrl Pts',(-20.1263232577722,25.4855037627183,-70.3018885573444));
#55142=CARTESIAN_POINT('Ctrl Pts',(-20.183409541383,25.586503258009,-70.2960351089956));
#55143=CARTESIAN_POINT('Ctrl Pts',(-20.2449453501414,25.6849336929597,-70.2901816606467));
#55144=CARTESIAN_POINT('Ctrl Pts',(-20.310658076488,25.780390815702,-70.2843282122979));
#55145=CARTESIAN_POINT('Ctrl Pts',(-20.376445532473,25.87595649392,-70.2784681073072));
#55146=CARTESIAN_POINT('Ctrl Pts',(-20.4464191524863,25.9685417702502,-70.2726080023166));
#55147=CARTESIAN_POINT('Ctrl Pts',(-20.5202646264403,26.0577736769719,-70.266747897326));
#55148=CARTESIAN_POINT('Ctrl Pts',(-20.5941598306995,26.1470656757985,-70.2608838459214));
#55149=CARTESIAN_POINT('Ctrl Pts',(-20.6719318041427,26.232999502574,-70.2550197945168));
#55150=CARTESIAN_POINT('Ctrl Pts',(-20.7532290157016,26.3152386891612,-70.2491557431122));
#55151=CARTESIAN_POINT('Ctrl Pts',(-20.8346460431168,26.3975990798878,-70.2432830492668));
#55152=CARTESIAN_POINT('Ctrl Pts',(-20.9195983756635,26.4762536831418,-70.2374103554213));
#55153=CARTESIAN_POINT('Ctrl Pts',(-21.0077009974478,26.5509059098273,-70.2315376615759));
#55154=CARTESIAN_POINT('Ctrl Pts',(-21.0318220143301,26.5713444346261,-70.2299298167182));
#55155=CARTESIAN_POINT('Ctrl Pts',(-21.0561790002685,26.5914832027443,-70.2283219718605));
#55156=CARTESIAN_POINT('Ctrl Pts',(-21.0807636899205,26.6113167029188,-70.2267141270027));
#55157=CARTESIAN_POINT('Ctrl Pts',(-21.1705538196383,26.6837541661788,-70.2208418300412));
#55158=CARTESIAN_POINT('Ctrl Pts',(-21.2636842842061,26.7523589143102,-70.2149695330797));
#55159=CARTESIAN_POINT('Ctrl Pts',(-21.359793845292,26.8168072523694,-70.2090972361182));
#55160=CARTESIAN_POINT('Ctrl Pts',(-21.4557788560196,26.8811720705008,-70.2032325491872));
#55161=CARTESIAN_POINT('Ctrl Pts',(-21.5547349456072,26.9413909620253,-70.1973678622562));
#55162=CARTESIAN_POINT('Ctrl Pts',(-21.6562675072221,26.9971801095634,-70.1915031753252));
#55163=CARTESIAN_POINT('Ctrl Pts',(-21.7576956489535,27.0529118814558,-70.1856445198576));
#55164=CARTESIAN_POINT('Ctrl Pts',(-21.8616946321271,27.104222773039,-70.1797858643899));
#55165=CARTESIAN_POINT('Ctrl Pts',(-21.967841104258,27.1508723497699,-70.1739272089223));
#55166=CARTESIAN_POINT('Ctrl Pts',(-22.0781337512672,27.1993441001372,-70.1678397092017));
#55167=CARTESIAN_POINT('Ctrl Pts',(-22.1907446953129,27.2427827086799,-70.1617522094811));
#55168=CARTESIAN_POINT('Ctrl Pts',(-22.3051707376551,27.2809710048777,-70.1556647097605));
#55169=CARTESIAN_POINT('Ctrl Pts',(-22.4151676762777,27.3176811417222,-70.1498128396842));
#55170=CARTESIAN_POINT('Ctrl Pts',(-22.5268413827651,27.3495397146062,-70.1439609696079));
#55171=CARTESIAN_POINT('Ctrl Pts',(-22.6397255129632,27.3764032799216,-70.1381090995316));
#55172=CARTESIAN_POINT('Ctrl Pts',(-22.7525924555269,27.403262755015,-70.1322581204557));
#55173=CARTESIAN_POINT('Ctrl Pts',(-22.8666690533158,27.4251286390516,-70.1264071413798));
#55174=CARTESIAN_POINT('Ctrl Pts',(-22.981476159631,27.4419080198615,-70.1205561623039));
#55175=CARTESIAN_POINT('Ctrl Pts',(-23.0962935882111,27.4586889092994,-70.1147046571686));
#55176=CARTESIAN_POINT('Ctrl Pts',(-23.2118412468211,27.470382326604,-70.1088531520333));
#55177=CARTESIAN_POINT('Ctrl Pts',(-23.3276329202268,27.4769470077886,-70.103001646898));
#55178=CARTESIAN_POINT('Ctrl Pts',(-23.4434630455278,27.4835138689609,-70.0971481986052));
#55179=CARTESIAN_POINT('Ctrl Pts',(-23.55953693425,27.4849485840369,-70.0912947503124));
#55180=CARTESIAN_POINT('Ctrl Pts',(-23.6753671265787,27.4812619870564,-70.0854413020195));
#55181=CARTESIAN_POINT('Ctrl Pts',(-23.7913290429907,27.4775711976145,-70.0795811970848));
#55182=CARTESIAN_POINT('Ctrl Pts',(-23.9070462964358,27.4687474846583,-70.0737210921501));
#55183=CARTESIAN_POINT('Ctrl Pts',(-24.0220352049937,27.4548536776724,-70.0678609872154));
#55184=CARTESIAN_POINT('Ctrl Pts',(-24.1371015513859,27.4409505140769,-70.0619969358667));
#55185=CARTESIAN_POINT('Ctrl Pts',(-24.2514381694125,27.4219705252512,-70.056132884518));
#55186=CARTESIAN_POINT('Ctrl Pts',(-24.364571965347,27.3980275848873,-70.0502688331694));
#55187=CARTESIAN_POINT('Ctrl Pts',(-24.477872497916,27.3740493574082,-70.0443961393794));
#55188=CARTESIAN_POINT('Ctrl Pts',(-24.5899662716441,27.3450936832612,-70.0385234455895));
#55189=CARTESIAN_POINT('Ctrl Pts',(-24.7003956437437,27.3113241637965,-70.0326507517995));
#55190=CARTESIAN_POINT('Ctrl Pts',(-24.7306293598649,27.3020786338652,-70.031042906409));
#55191=CARTESIAN_POINT('Ctrl Pts',(-24.7607384368583,27.2924725477748,-70.0294350610184));
#55192=CARTESIAN_POINT('Ctrl Pts',(-24.7907137702284,27.2825098802293,-70.0278272156279));
#55193=CARTESIAN_POINT('Ctrl Pts',(-24.9001919949714,27.2461234573288,-70.021954918668));
#55194=CARTESIAN_POINT('Ctrl Pts',(-25.0082512847691,27.2048550096705,-70.0160826217083));
#55195=CARTESIAN_POINT('Ctrl Pts',(-25.1144240450024,27.1588334822834,-70.0102103247485));
#55196=CARTESIAN_POINT('Ctrl Pts',(-25.2204592137675,27.1128715951421,-70.0043456378193));
#55197=CARTESIAN_POINT('Ctrl Pts',(-25.3246123389994,27.0621690404198,-69.9984809508901));
#55198=CARTESIAN_POINT('Ctrl Pts',(-25.426431338653,27.0069043921393,-69.992616263961));
#55199=CARTESIAN_POINT('Ctrl Pts',(-25.5281456238366,26.9516965800915,-69.9867576084954));
#55200=CARTESIAN_POINT('Ctrl Pts',(-25.6275301970324,26.8919362027846,-69.9808989530298));
#55201=CARTESIAN_POINT('Ctrl Pts',(-25.7241539366599,26.8278494687028,-69.9750402975642));
#55202=CARTESIAN_POINT('Ctrl Pts',(-25.8245518848761,26.7612594501992,-69.9689527978429));
#55203=CARTESIAN_POINT('Ctrl Pts',(-25.921968504259,26.6899983829722,-69.9628652981216));
#55204=CARTESIAN_POINT('Ctrl Pts',(-26.0159490853543,26.6143722266913,-69.9567777984003));
#55205=CARTESIAN_POINT('Ctrl Pts',(-26.1062919478126,26.5416733419268,-69.9509259283264));
#55206=CARTESIAN_POINT('Ctrl Pts',(-26.1934594722299,26.4649412882319,-69.9450740582525));
#55207=CARTESIAN_POINT('Ctrl Pts',(-26.2770788983064,26.3844908714159,-69.9392221881787));
#55208=CARTESIAN_POINT('Ctrl Pts',(-26.3606855925636,26.3040527039087,-69.9333712091053));
#55209=CARTESIAN_POINT('Ctrl Pts',(-26.4407449648164,26.2198975855049,-69.9275202300319));
#55210=CARTESIAN_POINT('Ctrl Pts',(-26.5169198473938,26.1323784073942,-69.9216692509586));
#55211=CARTESIAN_POINT('Ctrl Pts',(-26.5931015788251,26.0448513604684,-69.915817745826));
#55212=CARTESIAN_POINT('Ctrl Pts',(-26.6653978548847,25.9539599644044,-69.9099662406934));
#55213=CARTESIAN_POINT('Ctrl Pts',(-26.7335111395414,25.8600909753016,-69.9041147355608));
#55214=CARTESIAN_POINT('Ctrl Pts',(-26.8016470431362,25.7661908143523,-69.8982612872708));
#55215=CARTESIAN_POINT('Ctrl Pts',(-26.8655969505795,25.6693114286132,-69.8924078389809));
#55216=CARTESIAN_POINT('Ctrl Pts',(-26.9251064840354,25.5698687824624,-69.8865543906909));
#55217=CARTESIAN_POINT('Ctrl Pts',(-26.9846836927524,25.4703130484304,-69.8806942857592));
#55218=CARTESIAN_POINT('Ctrl Pts',(-27.0398102360944,25.368188590696,-69.8748341808275));
#55219=CARTESIAN_POINT('Ctrl Pts',(-27.0902775229772,25.2639363009736,-69.8689740758958));
#55220=CARTESIAN_POINT('Ctrl Pts',(-27.1407787964188,25.1596138038597,-69.8631100245503));
#55221=CARTESIAN_POINT('Ctrl Pts',(-27.186614402501,25.0531610002021,-69.8572459732048));
#55222=CARTESIAN_POINT('Ctrl Pts',(-27.2276244178556,24.9450374652483,-69.8513819218592));
#55223=CARTESIAN_POINT('Ctrl Pts',(-27.2686948737866,24.8367545777872,-69.8455092280726));
#55224=CARTESIAN_POINT('Ctrl Pts',(-27.3049254160151,24.7267964358507,-69.8396365342859));
#55225=CARTESIAN_POINT('Ctrl Pts',(-27.3362063097734,24.6156364954592,-69.8337638404993));
#55226=CARTESIAN_POINT('Ctrl Pts',(-27.3447704957242,24.5852027614637,-69.8321559950838));
#55227=CARTESIAN_POINT('Ctrl Pts',(-27.3529639669847,24.5546789925653,-69.8305481496684));
#55228=CARTESIAN_POINT('Ctrl Pts',(-27.3607851461743,24.5240749970254,-69.8289403042529));
#55229=CARTESIAN_POINT('Ctrl Pts',(-27.3982292934994,24.3775573824872,-69.8212426925305));
#55230=CARTESIAN_POINT('Ctrl Pts',(-27.4272382874208,24.2288027131749,-69.8135450808082));
#55231=CARTESIAN_POINT('Ctrl Pts',(-27.4475957085458,24.0786512086875,-69.8058474690858));
#55232=CARTESIAN_POINT('Ctrl Pts',(-27.4674978941642,23.9318574132038,-69.7983219924365));
#55233=CARTESIAN_POINT('Ctrl Pts',(-27.4791311547766,23.7837282753288,-69.7907965157872));
#55234=CARTESIAN_POINT('Ctrl Pts',(-27.4823378263443,23.6350713715633,-69.7832710391378));
#55235=CARTESIAN_POINT('Ctrl Pts',(-27.4829212395818,23.6080251325948,-69.7819018740694));
#55236=CARTESIAN_POINT('Ctrl Pts',(-27.4832258439406,23.5809614915974,-69.780532709001));
#55237=CARTESIAN_POINT('Ctrl Pts',(-27.4832508538687,23.5538854055544,-69.7791635439327));
#55238=CARTESIAN_POINT('',(-27.48082193576,23.5494884268893,-68.5291634982728));
#55239=CARTESIAN_POINT('Ctrl Pts',(-27.4825506534957,23.5538843258169,-69.7791635220347));
#55240=CARTESIAN_POINT('Ctrl Pts',(-27.4736068510643,22.571135203937,-69.7294601456491));
#55241=CARTESIAN_POINT('Ctrl Pts',(-26.6026245505,20.2634339527826,-69.6134611321385));
#55242=CARTESIAN_POINT('Ctrl Pts',(-22.7246114047614,18.9721451101221,-69.4311664815032));
#55243=CARTESIAN_POINT('Ctrl Pts',(-19.252319914895,21.7702171237683,-69.2322795701282));
#55244=CARTESIAN_POINT('Ctrl Pts',(-19.7294640953999,26.2039907547912,-69.0333926587533));
#55245=CARTESIAN_POINT('Ctrl Pts',(-23.7175888993554,28.1992039588933,-68.8345057473784));
#55246=CARTESIAN_POINT('Ctrl Pts',(-26.9579470188054,26.275131802411,-68.6664293684722));
#55247=CARTESIAN_POINT('Ctrl Pts',(-27.4756470504516,24.2536744838534,-68.564648626691));
#55248=CARTESIAN_POINT('Ctrl Pts',(-27.4768626123758,23.549489668419,-68.5291635220347));
#55249=CARTESIAN_POINT('',(-27.4835405418261,23.5468852840711,-67.2791635220347));
#55250=CARTESIAN_POINT('Ctrl Pts',(-27.4832524573208,23.5494876647477,-68.529163483686));
#55251=CARTESIAN_POINT('Ctrl Pts',(-27.4832283862113,23.425712317898,-68.5229363586002));
#55252=CARTESIAN_POINT('Ctrl Pts',(-27.4773570697139,23.302085006948,-68.5167092335144));
#55253=CARTESIAN_POINT('Ctrl Pts',(-27.4657057254873,23.1791524276579,-68.5104821084287));
#55254=CARTESIAN_POINT('Ctrl Pts',(-27.4540152803793,23.0558072974982,-68.5042340856616));
#55255=CARTESIAN_POINT('Ctrl Pts',(-27.4365060316608,22.9331618903031,-68.4979860628945));
#55256=CARTESIAN_POINT('Ctrl Pts',(-27.4132968556742,22.8117557131729,-68.4917380401273));
#55257=CARTESIAN_POINT('Ctrl Pts',(-27.3900487592371,22.6901459448813,-68.4854795397862));
#55258=CARTESIAN_POINT('Ctrl Pts',(-27.361081730058,22.5697798724058,-68.479221039445));
#55259=CARTESIAN_POINT('Ctrl Pts',(-27.3265646982176,22.4511822787225,-68.4729625391039));
#55260=CARTESIAN_POINT('Ctrl Pts',(-27.2919438843206,22.3322280986956,-68.4666852213847));
#55261=CARTESIAN_POINT('Ctrl Pts',(-27.2517397888736,22.2150533457786,-68.4604079036655));
#55262=CARTESIAN_POINT('Ctrl Pts',(-27.2061705425266,22.1001654660076,-68.4541305859463));
#55263=CARTESIAN_POINT('Ctrl Pts',(-27.1640695518829,21.9940216532599,-68.4483310321738));
#55264=CARTESIAN_POINT('Ctrl Pts',(-27.1173896272137,21.8898297857102,-68.4425314784013));
#55265=CARTESIAN_POINT('Ctrl Pts',(-27.0663369843744,21.7879701702037,-68.4367319246287));
#55266=CARTESIAN_POINT('Ctrl Pts',(-27.014643993578,21.6848329401982,-68.4308596276601));
#55267=CARTESIAN_POINT('Ctrl Pts',(-26.9583225723137,21.583799319875,-68.4249873306915));
#55268=CARTESIAN_POINT('Ctrl Pts',(-26.897567314718,21.4853136116894,-68.4191150337228));
#55269=CARTESIAN_POINT('Ctrl Pts',(-26.836890791111,21.3869555331601,-68.4132503467847));
#55270=CARTESIAN_POINT('Ctrl Pts',(-26.7717920727394,21.2911391490672,-68.4073856598465));
#55271=CARTESIAN_POINT('Ctrl Pts',(-26.70251264891,21.1982863003442,-68.4015209729084));
#55272=CARTESIAN_POINT('Ctrl Pts',(-26.633304474631,21.1055289449634,-68.3956623174336));
#55273=CARTESIAN_POINT('Ctrl Pts',(-26.5599243927277,21.0157293920309,-68.3898036619588));
#55274=CARTESIAN_POINT('Ctrl Pts',(-26.4826580333507,20.9292819149465,-68.3839450064841));
#55275=CARTESIAN_POINT('Ctrl Pts',(-26.4023735819201,20.8394577232641,-68.3778575067661));
#55276=CARTESIAN_POINT('Ctrl Pts',(-26.3178932996183,20.7532532029775,-68.3717700070482));
#55277=CARTESIAN_POINT('Ctrl Pts',(-26.2295851241246,20.6710745484601,-68.3656825073303));
#55278=CARTESIAN_POINT('Ctrl Pts',(-26.1446951045384,20.5920767936933,-68.3598306372469));
#55279=CARTESIAN_POINT('Ctrl Pts',(-26.05626834603,20.5167993482214,-68.3539787671636));
#55280=CARTESIAN_POINT('Ctrl Pts',(-25.9646698027029,20.4455660352094,-68.3481268970802));
#55281=CARTESIAN_POINT('Ctrl Pts',(-25.873085206087,20.3743435681171,-68.3422759179973));
#55282=CARTESIAN_POINT('Ctrl Pts',(-25.7783301111103,20.3071642628654,-68.3364249389144));
#55283=CARTESIAN_POINT('Ctrl Pts',(-25.6808020661824,20.2443112616332,-68.3305739598315));
#55284=CARTESIAN_POINT('Ctrl Pts',(-25.5832652525447,20.1814526093114,-68.3247224546892));
#55285=CARTESIAN_POINT('Ctrl Pts',(-25.4829553408366,20.1229212582056,-68.318870949547));
#55286=CARTESIAN_POINT('Ctrl Pts',(-25.3802977182725,20.0689562766935,-68.3130194444048));
#55287=CARTESIAN_POINT('Ctrl Pts',(-25.2776060053466,20.0149733745859,-68.3071659961051));
#55288=CARTESIAN_POINT('Ctrl Pts',(-25.1725653970445,19.9655600495693,-68.3013125478053));
#55289=CARTESIAN_POINT('Ctrl Pts',(-25.0656240056263,19.9209084730532,-68.2954590995056));
#55290=CARTESIAN_POINT('Ctrl Pts',(-24.9585609986243,19.8762061179987,-68.2895989945641));
#55291=CARTESIAN_POINT('Ctrl Pts',(-24.8495932757046,19.836276479274,-68.2837388896226));
#55292=CARTESIAN_POINT('Ctrl Pts',(-24.7391870608596,19.801262843077,-68.2778787846811));
#55293=CARTESIAN_POINT('Ctrl Pts',(-24.6287064943391,19.7662256273874,-68.2720147333258));
#55294=CARTESIAN_POINT('Ctrl Pts',(-24.5167859051605,19.7361111134737,-68.2661506819704));
#55295=CARTESIAN_POINT('Ctrl Pts',(-24.4039030369592,19.711011745437,-68.260286630615));
#55296=CARTESIAN_POINT('Ctrl Pts',(-24.2908538019437,19.6858753859421,-68.2544139368185));
#55297=CARTESIAN_POINT('Ctrl Pts',(-24.1768398630102,19.6657689955036,-68.2485412430219));
#55298=CARTESIAN_POINT('Ctrl Pts',(-24.0623455123509,19.6507333588779,-68.2426685492254));
#55299=CARTESIAN_POINT('Ctrl Pts',(-24.0309988743857,19.6466168530837,-68.2410607039015));
#55300=CARTESIAN_POINT('Ctrl Pts',(-23.9996162315936,19.6428801357629,-68.2394528585776));
#55301=CARTESIAN_POINT('Ctrl Pts',(-23.9682075170356,19.6395233630828,-68.2378450132537));
#55302=CARTESIAN_POINT('Ctrl Pts',(-23.8534941820222,19.627263498442,-68.2319727162851));
#55303=CARTESIAN_POINT('Ctrl Pts',(-23.7380487862485,19.6200347002225,-68.2261004193164));
#55304=CARTESIAN_POINT('Ctrl Pts',(-23.6223503152049,19.6179134174248,-68.2202281223477));
#55305=CARTESIAN_POINT('Ctrl Pts',(-23.5068017801913,19.6157948836412,-68.2143634354095));
#55306=CARTESIAN_POINT('Ctrl Pts',(-23.3910012316118,19.6187707101027,-68.2084987484713));
#55307=CARTESIAN_POINT('Ctrl Pts',(-23.2754341065293,19.6268657507115,-68.2026340615331));
#55308=CARTESIAN_POINT('Ctrl Pts',(-23.1599858350003,19.6349524660778,-68.1967754060583));
#55309=CARTESIAN_POINT('Ctrl Pts',(-23.044770919367,19.6481478949392,-68.1909167505835));
#55310=CARTESIAN_POINT('Ctrl Pts',(-22.9302754636613,19.6664248533447,-68.1850580951087));
#55311=CARTESIAN_POINT('Ctrl Pts',(-22.8113077146091,19.6854157258438,-68.1789705953908));
#55312=CARTESIAN_POINT('Ctrl Pts',(-22.6931172313741,19.7098932070916,-68.1728830956729));
#55313=CARTESIAN_POINT('Ctrl Pts',(-22.5762446380117,19.7397673102238,-68.166795595955));
#55314=CARTESIAN_POINT('Ctrl Pts',(-22.4638958471521,19.7684850726039,-68.1609437258716));
#55315=CARTESIAN_POINT('Ctrl Pts',(-22.3527652576022,19.8021893376685,-68.1550918557882));
#55316=CARTESIAN_POINT('Ctrl Pts',(-22.2433225803882,19.8407481035557,-68.1492399857048));
#55317=CARTESIAN_POINT('Ctrl Pts',(-22.1338965668171,19.8793009985201,-68.1433890066219));
#55318=CARTESIAN_POINT('Ctrl Pts',(-22.0261583443687,19.9227067873276,-68.1375380275389));
#55319=CARTESIAN_POINT('Ctrl Pts',(-21.9205610170775,19.9707840561819,-68.131687048456));
#55320=CARTESIAN_POINT('Ctrl Pts',(-21.8149541955703,20.0188656476454,-68.1258355433137));
#55321=CARTESIAN_POINT('Ctrl Pts',(-21.7114890281137,20.0716193827978,-68.1199840381714));
#55322=CARTESIAN_POINT('Ctrl Pts',(-21.6105965867679,20.1288166028316,-68.1141325330291));
#55323=CARTESIAN_POINT('Ctrl Pts',(-21.5096706412387,20.1860328168169,-68.1082790847294));
#55324=CARTESIAN_POINT('Ctrl Pts',(-21.4113194800582,20.2476952460285,-68.1024256364296));
#55325=CARTESIAN_POINT('Ctrl Pts',(-21.3159470039309,20.3135307628969,-68.0965721881299));
#55326=CARTESIAN_POINT('Ctrl Pts',(-21.2204660685884,20.3794411490438,-68.0907120831884));
#55327=CARTESIAN_POINT('Ctrl Pts',(-21.127970919872,20.4495338601562,-68.0848519782468));
#55328=CARTESIAN_POINT('Ctrl Pts',(-21.0388341206963,20.5234941064311,-68.0789918733053));
#55329=CARTESIAN_POINT('Ctrl Pts',(-20.9496372934653,20.5975041603029,-68.0731278219499));
#55330=CARTESIAN_POINT('Ctrl Pts',(-20.8638036245391,20.675386658396,-68.0672637705945));
#55331=CARTESIAN_POINT('Ctrl Pts',(-20.7816691293789,20.75678963693,-68.0613997192391));
#55332=CARTESIAN_POINT('Ctrl Pts',(-20.6994135843686,20.8383125872047,-68.0555270254425));
#55333=CARTESIAN_POINT('Ctrl Pts',(-20.620868373355,20.9233660705823,-68.0496543316459));
#55334=CARTESIAN_POINT('Ctrl Pts',(-20.5463295896988,21.0115646898055,-68.0437816378494));
#55335=CARTESIAN_POINT('Ctrl Pts',(-20.5259221176133,21.0357119963684,-68.0421737925259));
#55336=CARTESIAN_POINT('Ctrl Pts',(-20.5058147058072,21.0600948861663,-68.0405659472024));
#55337=CARTESIAN_POINT('Ctrl Pts',(-20.4860128549072,21.0847050867635,-68.0389581018789));
#55338=CARTESIAN_POINT('Ctrl Pts',(-20.4136910044672,21.1745883636287,-68.0330858049102));
#55339=CARTESIAN_POINT('Ctrl Pts',(-20.3452061647447,21.2678070401771,-68.0272135079415));
#55340=CARTESIAN_POINT('Ctrl Pts',(-20.2808815655298,21.3639994618046,-68.0213412109727));
#55341=CARTESIAN_POINT('Ctrl Pts',(-20.216640325887,21.4600672256932,-68.0154765240345));
#55342=CARTESIAN_POINT('Ctrl Pts',(-20.156548832977,21.5591007305008,-68.0096118370963));
#55343=CARTESIAN_POINT('Ctrl Pts',(-20.1008903961162,21.6607050044695,-68.003747150158));
#55344=CARTESIAN_POINT('Ctrl Pts',(-20.0452892004735,21.7622047848029,-67.9978884946832));
#55345=CARTESIAN_POINT('Ctrl Pts',(-19.994112189964,21.8662697151237,-67.9920298392084));
#55346=CARTESIAN_POINT('Ctrl Pts',(-19.94759925411,21.9724761338761,-67.9861711837335));
#55347=CARTESIAN_POINT('Ctrl Pts',(-19.8992694820138,22.0828310688898,-67.9800836840156));
#55348=CARTESIAN_POINT('Ctrl Pts',(-19.8559758310383,22.1954978217528,-67.9739961842977));
#55349=CARTESIAN_POINT('Ctrl Pts',(-19.8179348239456,22.3099729146617,-67.9679086845798));
#55350=CARTESIAN_POINT('Ctrl Pts',(-19.7813662750067,22.4200170054272,-67.9620568144964));
#55351=CARTESIAN_POINT('Ctrl Pts',(-19.7496514438923,22.5317316190854,-67.9562049444129));
#55352=CARTESIAN_POINT('Ctrl Pts',(-19.7229331739432,22.6446502272666,-67.9503530743295));
#55353=CARTESIAN_POINT('Ctrl Pts',(-19.6962189720937,22.757551642563,-67.9445020952465));
#55354=CARTESIAN_POINT('Ctrl Pts',(-19.6744999139099,22.8716562857205,-67.9386511161635));
#55355=CARTESIAN_POINT('Ctrl Pts',(-19.6578682948601,22.9864848908653,-67.9328001370805));
#55356=CARTESIAN_POINT('Ctrl Pts',(-19.6412351804678,23.1013238202067,-67.9269486319382));
#55357=CARTESIAN_POINT('Ctrl Pts',(-19.629690473757,23.2168864317923,-67.9210971267959));
#55358=CARTESIAN_POINT('Ctrl Pts',(-19.6232748129593,23.332686457686,-67.9152456216535));
#55359=CARTESIAN_POINT('Ctrl Pts',(-19.6168570216602,23.4485249382475,-67.9093921733537));
#55360=CARTESIAN_POINT('Ctrl Pts',(-19.6155716859241,23.5646005773543,-67.903538725054));
#55361=CARTESIAN_POINT('Ctrl Pts',(-19.6194073443974,23.6804259295369,-67.8976852767542));
#55362=CARTESIAN_POINT('Ctrl Pts',(-19.6232473648473,23.796383000296,-67.8918251718126));
#55363=CARTESIAN_POINT('Ctrl Pts',(-19.6322199897106,23.9120888026154,-67.885965066871));
#55364=CARTESIAN_POINT('Ctrl Pts',(-19.646261767094,24.0270597358308,-67.8801049619294));
#55365=CARTESIAN_POINT('Ctrl Pts',(-19.6603130007356,24.1421080947738,-67.874240910574));
#55366=CARTESIAN_POINT('Ctrl Pts',(-19.6794401163117,24.2564201924733,-67.8683768592185));
#55367=CARTESIAN_POINT('Ctrl Pts',(-19.7035286313899,24.3695230821397,-67.862512807863));
#55368=CARTESIAN_POINT('Ctrl Pts',(-19.7276526481307,24.482792662888,-67.8566401140664));
#55369=CARTESIAN_POINT('Ctrl Pts',(-19.7567525544247,24.5948490802039,-67.8507674202698));
#55370=CARTESIAN_POINT('Ctrl Pts',(-19.7906641601067,24.7052349022195,-67.8448947264732));
#55371=CARTESIAN_POINT('Ctrl Pts',(-19.7999485904692,24.7354566937536,-67.8432868811501));
#55372=CARTESIAN_POINT('Ctrl Pts',(-19.8095934162612,24.7655533822659,-67.841679035827));
#55373=CARTESIAN_POINT('Ctrl Pts',(-19.8195946510658,24.7955158683845,-67.8400711905039));
#55374=CARTESIAN_POINT('Ctrl Pts',(-19.8561219338723,24.9049471761611,-67.8341988935352));
#55375=CARTESIAN_POINT('Ctrl Pts',(-19.8975294113498,25.0129532673691,-67.8283265965665));
#55376=CARTESIAN_POINT('Ctrl Pts',(-19.9436875368159,25.1190667137178,-67.8224542995978));
#55377=CARTESIAN_POINT('Ctrl Pts',(-19.9897858450172,25.2250426454674,-67.8165896126596));
#55378=CARTESIAN_POINT('Ctrl Pts',(-20.040622394843,25.3291304343588,-67.8107249257215));
#55379=CARTESIAN_POINT('Ctrl Pts',(-20.0960180306221,25.4308782285311,-67.8048602387833));
#55380=CARTESIAN_POINT('Ctrl Pts',(-20.1513566954577,25.5325213814667,-67.7990015833085));
#55381=CARTESIAN_POINT('Ctrl Pts',(-20.2112449236353,25.6318289655324,-67.7931429278336));
#55382=CARTESIAN_POINT('Ctrl Pts',(-20.2754559520363,25.7283701506168,-67.7872842723588));
#55383=CARTESIAN_POINT('Ctrl Pts',(-20.3421751197632,25.8286823194232,-67.7811967726409));
#55384=CARTESIAN_POINT('Ctrl Pts',(-20.4135614955971,25.9260071505859,-67.775109272923));
#55385=CARTESIAN_POINT('Ctrl Pts',(-20.4893085349464,26.0198903287757,-67.7690217732051));
#55386=CARTESIAN_POINT('Ctrl Pts',(-20.5621236239015,26.1101395587127,-67.7631699031217));
#55387=CARTESIAN_POINT('Ctrl Pts',(-20.6389677920425,26.1972082628491,-67.7573180330384));
#55388=CARTESIAN_POINT('Ctrl Pts',(-20.7195257541058,26.2807240863242,-67.751466162955));
#55389=CARTESIAN_POINT('Ctrl Pts',(-20.8000714504867,26.3642271937558,-67.745615183872));
#55390=CARTESIAN_POINT('Ctrl Pts',(-20.8843295295658,26.4441781986792,-67.7397642047891));
#55391=CARTESIAN_POINT('Ctrl Pts',(-20.9719466665354,26.5202403878457,-67.7339132257061));
#55392=CARTESIAN_POINT('Ctrl Pts',(-21.0595716811287,26.5963094157351,-67.7280617205638));
#55393=CARTESIAN_POINT('Ctrl Pts',(-21.150556041801,26.6684886617996,-67.7222102154216));
#55394=CARTESIAN_POINT('Ctrl Pts',(-21.2445126098657,26.7364810879793,-67.7163587102793));
#55395=CARTESIAN_POINT('Ctrl Pts',(-21.3385003788614,26.8044960929636,-67.7105052619795));
#55396=CARTESIAN_POINT('Ctrl Pts',(-21.4354619831323,26.8683212712168,-67.7046518136798));
#55397=CARTESIAN_POINT('Ctrl Pts',(-21.5349811312791,26.9277027804276,-67.69879836538));
#55398=CARTESIAN_POINT('Ctrl Pts',(-21.6346134543076,26.9871518193087,-67.6929382604385));
#55399=CARTESIAN_POINT('Ctrl Pts',(-21.7368087712538,27.0421468907372,-67.687078155497));
#55400=CARTESIAN_POINT('Ctrl Pts',(-21.8411259223268,27.092479971195,-67.6812180505554));
#55401=CARTESIAN_POINT('Ctrl Pts',(-21.945513324472,27.1428469478322,-67.6753539992));
#55402=CARTESIAN_POINT('Ctrl Pts',(-22.0520250270473,27.1885455194192,-67.6694899478446));
#55403=CARTESIAN_POINT('Ctrl Pts',(-22.1602012493755,27.2294163541577,-67.6636258964892));
#55404=CARTESIAN_POINT('Ctrl Pts',(-22.2685369018614,27.270347424348,-67.6577532026926));
#55405=CARTESIAN_POINT('Ctrl Pts',(-22.3785415788432,27.3064364289057,-67.651880508896));
#55406=CARTESIAN_POINT('Ctrl Pts',(-22.4897416834709,27.3375742424551,-67.6460078150995));
#55407=CARTESIAN_POINT('Ctrl Pts',(-22.5201864119694,27.3460992549335,-67.644399969776));
#55408=CARTESIAN_POINT('Ctrl Pts',(-22.5507206982046,27.3542534372032,-67.6427921244526));
#55409=CARTESIAN_POINT('Ctrl Pts',(-22.5813347318949,27.3620352245077,-67.6411842791292));
#55410=CARTESIAN_POINT('Ctrl Pts',(-22.6931456720514,27.3904564695944,-67.6353119821605));
#55411=CARTESIAN_POINT('Ctrl Pts',(-22.8063955057018,27.4140015350489,-67.6294396851918));
#55412=CARTESIAN_POINT('Ctrl Pts',(-22.920620952109,27.4325267458616,-67.6235673882231));
#55413=CARTESIAN_POINT('Ctrl Pts',(-23.0346983714093,27.4510279494723,-67.6177027012849));
#55414=CARTESIAN_POINT('Ctrl Pts',(-23.1497484849095,27.464522169646,-67.6118380143466));
#55415=CARTESIAN_POINT('Ctrl Pts',(-23.2652943008228,27.4729158879687,-67.6059733274084));
#55416=CARTESIAN_POINT('Ctrl Pts',(-23.3807212850978,27.4813009738775,-67.6001146719336));
#55417=CARTESIAN_POINT('Ctrl Pts',(-23.4966425479518,27.484595961827,-67.5942560164588));
#55418=CARTESIAN_POINT('Ctrl Pts',(-23.6125730497049,27.4827587494941,-67.588397360984));
#55419=CARTESIAN_POINT('Ctrl Pts',(-23.7330318989666,27.4808497740293,-67.5823098612661));
#55420=CARTESIAN_POINT('Ctrl Pts',(-23.8535002747853,27.4733994154378,-67.5762223615482));
#55421=CARTESIAN_POINT('Ctrl Pts',(-23.9734302537047,27.4604199981327,-67.5701348618303));
#55422=CARTESIAN_POINT('Ctrl Pts',(-24.0887180875057,27.4479429768025,-67.5642829917469));
#55423=CARTESIAN_POINT('Ctrl Pts',(-24.2035079796918,27.430357014525,-67.5584311216635));
#55424=CARTESIAN_POINT('Ctrl Pts',(-24.3173162368203,27.4077260924951,-67.5525792515801));
#55425=CARTESIAN_POINT('Ctrl Pts',(-24.4311071656067,27.3850986162289,-67.5467282724971));
#55426=CARTESIAN_POINT('Ctrl Pts',(-24.5439163511823,27.3574277881214,-67.5408772934141));
#55427=CARTESIAN_POINT('Ctrl Pts',(-24.6552695240046,27.3248288584765,-67.5350263143312));
#55428=CARTESIAN_POINT('Ctrl Pts',(-24.7666327085487,27.292226997874,-67.5291748091889));
#55429=CARTESIAN_POINT('Ctrl Pts',(-24.8765392233482,27.2546962710756,-67.5233233040466));
#55430=CARTESIAN_POINT('Ctrl Pts',(-24.9845299004276,27.2124018226897,-67.5174717989043));
#55431=CARTESIAN_POINT('Ctrl Pts',(-25.09255643886,27.1700933292383,-67.5116183506045));
#55432=CARTESIAN_POINT('Ctrl Pts',(-25.1986654898017,27.1230181193066,-67.5057649023047));
#55433=CARTESIAN_POINT('Ctrl Pts',(-25.3024184683078,27.071389213303,-67.499911454005));
#55434=CARTESIAN_POINT('Ctrl Pts',(-25.4062894364801,27.0197015940222,-67.4940513490635));
#55435=CARTESIAN_POINT('Ctrl Pts',(-25.5077986139703,26.9634501267305,-67.4881912441219));
#55436=CARTESIAN_POINT('Ctrl Pts',(-25.6065325215332,26.9028935210319,-67.4823311391804));
#55437=CARTESIAN_POINT('Ctrl Pts',(-25.7053329202034,26.8422961342495,-67.476467087825));
#55438=CARTESIAN_POINT('Ctrl Pts',(-25.801353985815,26.7773880670358,-67.4706030364695));
#55439=CARTESIAN_POINT('Ctrl Pts',(-25.8942131389054,26.7084700149974,-67.4647389851141));
#55440=CARTESIAN_POINT('Ctrl Pts',(-25.9872091478511,26.6394503915076,-67.4588662913175));
#55441=CARTESIAN_POINT('Ctrl Pts',(-26.0770336242338,26.5664092479619,-67.4529935975209));
#55442=CARTESIAN_POINT('Ctrl Pts',(-26.1633387598692,26.4896860424446,-67.4471209037243));
#55443=CARTESIAN_POINT('Ctrl Pts',(-26.1869676622981,26.4686805121959,-67.445513058401));
#55444=CARTESIAN_POINT('Ctrl Pts',(-26.2103329888039,26.4473991860725,-67.4439052130776));
#55445=CARTESIAN_POINT('Ctrl Pts',(-26.2334281200576,26.4258494718113,-67.4422973677542));
#55446=CARTESIAN_POINT('Ctrl Pts',(-26.316523802111,26.3483141599345,-67.4365123820655));
#55447=CARTESIAN_POINT('Ctrl Pts',(-26.3964150326815,26.2670252898223,-67.4307273963768));
#55448=CARTESIAN_POINT('Ctrl Pts',(-26.4727356899813,26.1822823927573,-67.424942410688));
#55449=CARTESIAN_POINT('Ctrl Pts',(-26.552870868075,26.0933040297723,-67.4188682903275));
#55450=CARTESIAN_POINT('Ctrl Pts',(-26.629068918564,26.0005176697059,-67.4127941699669));
#55451=CARTESIAN_POINT('Ctrl Pts',(-26.7009452846778,25.9043179887911,-67.4067200496064));
#55452=CARTESIAN_POINT('Ctrl Pts',(-26.7692293025233,25.8129263244166,-67.4009495110341));
#55453=CARTESIAN_POINT('Ctrl Pts',(-26.8336128432904,25.7184546498319,-67.3951789724618));
#55454=CARTESIAN_POINT('Ctrl Pts',(-26.8938048520551,25.6212780943102,-67.3894084338895));
#55455=CARTESIAN_POINT('Ctrl Pts',(-26.953959458448,25.5241619227786,-67.3836414810395));
#55456=CARTESIAN_POINT('Ctrl Pts',(-27.0099274837551,25.4243445712755,-67.3778745281896));
#55457=CARTESIAN_POINT('Ctrl Pts',(-27.0614603196305,25.3222313323392,-67.3721075753396));
#55458=CARTESIAN_POINT('Ctrl Pts',(-27.1129744756948,25.2201551077839,-67.3663427129158));
#55459=CARTESIAN_POINT('Ctrl Pts',(-27.1600564460019,25.1157850305423,-67.360577850492));
#55460=CARTESIAN_POINT('Ctrl Pts',(-27.202503292056,25.0095514672919,-67.3548129880683));
#55461=CARTESIAN_POINT('Ctrl Pts',(-27.2449457395983,24.903328912388,-67.3490487230226));
#55462=CARTESIAN_POINT('Ctrl Pts',(-27.2827538613391,24.7952436522743,-67.3432844579769));
#55463=CARTESIAN_POINT('Ctrl Pts',(-27.3157729852035,24.6857456907238,-67.3375201929312));
#55464=CARTESIAN_POINT('Ctrl Pts',(-27.3488106043595,24.5761863951192,-67.3317526990971));
#55465=CARTESIAN_POINT('Ctrl Pts',(-27.3770537451572,24.4652132267656,-67.3259852052631));
#55466=CARTESIAN_POINT('Ctrl Pts',(-27.4003978176522,24.353290685841,-67.320217711429));
#55467=CARTESIAN_POINT('Ctrl Pts',(-27.4237495032394,24.2413316441459,-67.3144483366694));
#55468=CARTESIAN_POINT('Ctrl Pts',(-27.442198868346,24.1284230341177,-67.3086789619098));
#55469=CARTESIAN_POINT('Ctrl Pts',(-27.4556928575527,24.0150372788176,-67.3029095871502));
#55470=CARTESIAN_POINT('Ctrl Pts',(-27.4692011758476,23.9015311206873,-67.297134085968));
#55471=CARTESIAN_POINT('Ctrl Pts',(-27.4777435827243,23.7875472309409,-67.2913585847858));
#55472=CARTESIAN_POINT('Ctrl Pts',(-27.4813190681306,23.6735606259547,-67.2855830836036));
#55473=CARTESIAN_POINT('Ctrl Pts',(-27.4826438044597,23.6313279835306,-67.2834432297473));
#55474=CARTESIAN_POINT('Ctrl Pts',(-27.4832872255155,23.5890949466114,-67.281303375891));
#55475=CARTESIAN_POINT('Ctrl Pts',(-27.4832510904674,23.5468855318674,-67.2791635220347));
#55476=CARTESIAN_POINT('',(-27.4879913355201,23.552603565581,-66.0291635220347));
#55477=CARTESIAN_POINT('Ctrl Pts',(-27.4853590703307,23.5468837272474,-67.2791635220347));
#55478=CARTESIAN_POINT('Ctrl Pts',(-27.4874959140799,23.3116748807435,-67.2672458334829));
#55479=CARTESIAN_POINT('Ctrl Pts',(-27.3610477196202,21.7703416614824,-67.189032507806));
#55480=CARTESIAN_POINT('Ctrl Pts',(-25.3247553604629,19.2500327067552,-67.0445235450044));
#55481=CARTESIAN_POINT('Ctrl Pts',(-20.8915994482856,19.7328824141667,-66.8456366336297));
#55482=CARTESIAN_POINT('Ctrl Pts',(-18.9015203031529,23.7235715999746,-66.6467497222545));
#55483=CARTESIAN_POINT('Ctrl Pts',(-21.1832319285545,27.554995257066,-66.4478628108798));
#55484=CARTESIAN_POINT('Ctrl Pts',(-25.6400347979899,27.7063998957303,-66.2489758995048));
#55485=CARTESIAN_POINT('Ctrl Pts',(-27.4199713476433,25.1326070363992,-66.1094094698899));
#55486=CARTESIAN_POINT('Ctrl Pts',(-27.4889610422656,23.6900265544838,-66.0361386773998));
#55487=CARTESIAN_POINT('Ctrl Pts',(-27.4879913355201,23.552603565581,-66.0291635220347));
#55488=CARTESIAN_POINT('',(-27.4779966819508,23.5524812139231,-64.7791635220347));
#55489=CARTESIAN_POINT('Ctrl Pts',(-27.4879913355201,23.552603565581,-66.0291635220347));
#55490=CARTESIAN_POINT('Ctrl Pts',(-27.4797444265551,22.3838843787112,-65.9698430402749));
#55491=CARTESIAN_POINT('Ctrl Pts',(-26.3078739937543,19.894666085494,-65.8442269213898));
#55492=CARTESIAN_POINT('Ctrl Pts',(-22.0716745106532,19.1395204079076,-65.6523151653804));
#55493=CARTESIAN_POINT('Ctrl Pts',(-19.0401954898553,22.4100173316296,-65.4534282540051));
#55494=CARTESIAN_POINT('Ctrl Pts',(-20.153076500729,26.7282937282087,-65.2545413426305));
#55495=CARTESIAN_POINT('Ctrl Pts',(-24.3876742510315,28.1262197186492,-65.0556544312555));
#55496=CARTESIAN_POINT('Ctrl Pts',(-27.1484078217908,25.8897972304457,-64.8971951577236));
#55497=CARTESIAN_POINT('Ctrl Pts',(-27.4806287621626,24.0654490020844,-64.8050315213167));
#55498=CARTESIAN_POINT('Ctrl Pts',(-27.4779966819508,23.5524812139231,-64.7791635220347));
#55499=CARTESIAN_POINT('',(-27.4798202215753,23.5470868039979,-63.5291635220347));
#55500=CARTESIAN_POINT('Ctrl Pts',(-27.4779966819508,23.5524812139231,-64.7791635220347));
#55501=CARTESIAN_POINT('Ctrl Pts',(-27.4738831521638,22.7507927749053,-64.7387358841917));
#55502=CARTESIAN_POINT('Ctrl Pts',(-26.8448208971909,20.6285198012337,-64.6320126092237));
#55503=CARTESIAN_POINT('Ctrl Pts',(-23.3709510498503,18.9017472008681,-64.4589936971309));
#55504=CARTESIAN_POINT('Ctrl Pts',(-19.5424669510336,21.1883876812941,-64.2601067857559));
#55505=CARTESIAN_POINT('Ctrl Pts',(-19.3967979966629,25.6453817061212,-64.061219874381));
#55506=CARTESIAN_POINT('Ctrl Pts',(-23.0678016051148,28.1771296573105,-63.8623329630061));
#55507=CARTESIAN_POINT('Ctrl Pts',(-26.7366505891984,26.6434011874026,-63.6849808455575));
#55508=CARTESIAN_POINT('Ctrl Pts',(-27.473158079598,24.4336695320874,-63.5739243652336));
#55509=CARTESIAN_POINT('Ctrl Pts',(-27.4798202215753,23.5470868039979,-63.5291635220347));
#55510=CARTESIAN_POINT('',(-27.4855958674576,23.5492949760936,-62.2791639176179));
#55511=CARTESIAN_POINT('Ctrl Pts',(-27.4798202215753,23.5470868039979,-63.5291635220347));
#55512=CARTESIAN_POINT('Ctrl Pts',(-27.4830254305109,23.1205448762016,-63.5076287281086));
#55513=CARTESIAN_POINT('Ctrl Pts',(-27.2221533585443,21.3846924303558,-63.4197982970575));
#55514=CARTESIAN_POINT('Ctrl Pts',(-24.6846826946482,19.0387318304793,-63.2656722288816));
#55515=CARTESIAN_POINT('Ctrl Pts',(-20.3678420653385,20.157169205907,-63.0667853175066));
#55516=CARTESIAN_POINT('Ctrl Pts',(-18.9753668306978,24.393562471708,-62.8678984061318));
#55517=CARTESIAN_POINT('Ctrl Pts',(-21.786823668931,27.8550254035288,-62.6690114947568));
#55518=CARTESIAN_POINT('Ctrl Pts',(-26.1598424050956,27.3673334894723,-62.4727668831467));
#55519=CARTESIAN_POINT('Ctrl Pts',(-27.4853352952305,24.8021464490294,-62.3428179086613));
#55520=CARTESIAN_POINT('Ctrl Pts',(-27.4894683157168,23.5493068921072,-62.2791645713009));
#55521=CARTESIAN_POINT('',(-27.4832508498222,23.5538897837606,-61.0291635375734));
#55522=CARTESIAN_POINT('Ctrl Pts',(-27.4832524133653,23.5492877649886,-62.2791635220346));
#55523=CARTESIAN_POINT('Ctrl Pts',(-27.4832396780116,23.4973704005476,-62.2765215720254));
#55524=CARTESIAN_POINT('Ctrl Pts',(-27.4821989889277,23.445466886612,-62.2738796220162));
#55525=CARTESIAN_POINT('Ctrl Pts',(-27.480131717455,23.393604565465,-62.271237672007));
#55526=CARTESIAN_POINT('Ctrl Pts',(-27.4755367660139,23.2783295034084,-62.2653653750383));
#55527=CARTESIAN_POINT('Ctrl Pts',(-27.4658577751254,23.1630636712445,-62.2594930780696));
#55528=CARTESIAN_POINT('Ctrl Pts',(-27.4510889429275,23.0482920822599,-62.2536207811009));
#55529=CARTESIAN_POINT('Ctrl Pts',(-27.4363392499632,22.9336692281397,-62.2477560941628));
#55530=CARTESIAN_POINT('Ctrl Pts',(-27.4165128850979,22.8195397496921,-62.2418914072246));
#55531=CARTESIAN_POINT('Ctrl Pts',(-27.39165603088,22.7063875208997,-62.2360267202864));
#55532=CARTESIAN_POINT('Ctrl Pts',(-27.3668247403806,22.5933516620911,-62.2301680648116));
#55533=CARTESIAN_POINT('Ctrl Pts',(-27.3369733391347,22.4812914551893,-62.2243094093368));
#55534=CARTESIAN_POINT('Ctrl Pts',(-27.3021995888,22.3706838475238,-62.218450753862));
#55535=CARTESIAN_POINT('Ctrl Pts',(-27.2660675451487,22.2557558092808,-62.2123632541441));
#55536=CARTESIAN_POINT('Ctrl Pts',(-27.2246208285365,22.1423966142518,-62.2062757544262));
#55537=CARTESIAN_POINT('Ctrl Pts',(-27.1780272809046,22.0311279913778,-62.2001882547082));
#55538=CARTESIAN_POINT('Ctrl Pts',(-27.1332372357135,21.9241662574001,-62.1943363846249));
#55539=CARTESIAN_POINT('Ctrl Pts',(-27.0836915635299,21.8191366816362,-62.1884845145415));
#55540=CARTESIAN_POINT('Ctrl Pts',(-27.0295893341285,21.7164847123599,-62.1826326444581));
#55541=CARTESIAN_POINT('Ctrl Pts',(-26.9754953422835,21.6138483727794,-62.1767816653751));
#55542=CARTESIAN_POINT('Ctrl Pts',(-26.9168463653594,21.51358928549,-62.1709306862922));
#55543=CARTESIAN_POINT('Ctrl Pts',(-26.8538879360401,21.4161292655373,-62.1650797072092));
#55544=CARTESIAN_POINT('Ctrl Pts',(-26.7909238461521,21.3186604829907,-62.1592282020669));
#55545=CARTESIAN_POINT('Ctrl Pts',(-26.7236497579546,21.2239916153172,-62.1533766969246));
#55546=CARTESIAN_POINT('Ctrl Pts',(-26.6523547323724,21.1325157932243,-62.1475251917823));
#55547=CARTESIAN_POINT('Ctrl Pts',(-26.5810360312643,21.0410095940021,-62.1416717434826));
#55548=CARTESIAN_POINT('Ctrl Pts',(-26.5056939916643,20.9526988746596,-62.1358182951828));
#55549=CARTESIAN_POINT('Ctrl Pts',(-26.42665770689,20.8679434018386,-62.129964846883));
#55550=CARTESIAN_POINT('Ctrl Pts',(-26.3475315406976,20.7830915436407,-62.1241047419415));
#55551=CARTESIAN_POINT('Ctrl Pts',(-26.2647030260392,20.701803304352,-62.118244637));
#55552=CARTESIAN_POINT('Ctrl Pts',(-26.178537904666,20.6244013737877,-62.1123845320584));
#55553=CARTESIAN_POINT('Ctrl Pts',(-26.0923147564763,20.5469473178676,-62.106520480703));
#55554=CARTESIAN_POINT('Ctrl Pts',(-26.0027508460223,20.4733850437404,-62.1006564293475));
#55555=CARTESIAN_POINT('Ctrl Pts',(-25.9102433636795,20.4039956647259,-62.0947923779921));
#55556=CARTESIAN_POINT('Ctrl Pts',(-25.8175995437741,20.3345040196182,-62.0889196841955));
#55557=CARTESIAN_POINT('Ctrl Pts',(-25.7220038337499,20.2691977761741,-62.083046990399));
#55558=CARTESIAN_POINT('Ctrl Pts',(-25.6238806800869,20.2083136779458,-62.0771742966024));
#55559=CARTESIAN_POINT('Ctrl Pts',(-25.5970162020123,20.1916446303164,-62.075566451279));
#55560=CARTESIAN_POINT('Ctrl Pts',(-25.5699624029027,20.1753067822909,-62.0739586059556));
#55561=CARTESIAN_POINT('Ctrl Pts',(-25.5427282687353,20.1593043697043,-62.0723507606321));
#55562=CARTESIAN_POINT('Ctrl Pts',(-25.443261658866,20.1008591215487,-62.0664784636635));
#55563=CARTESIAN_POINT('Ctrl Pts',(-25.3410546754112,20.0466961502296,-62.0606061666948));
#55564=CARTESIAN_POINT('Ctrl Pts',(-25.2365122320342,19.9970825071936,-62.0547338697261));
#55565=CARTESIAN_POINT('Ctrl Pts',(-25.1321052673613,19.9475331594989,-62.0488691827879));
#55566=CARTESIAN_POINT('Ctrl Pts',(-25.025369231542,19.9025215915189,-62.0430044958497));
#55567=CARTESIAN_POINT('Ctrl Pts',(-24.9167361795013,19.862270503501,-62.0371398089115));
#55568=CARTESIAN_POINT('Ctrl Pts',(-24.8082148497541,19.8220608112075,-62.0312811534367));
#55569=CARTESIAN_POINT('Ctrl Pts',(-24.6978007696496,19.7866020035299,-62.0254224979619));
#55570=CARTESIAN_POINT('Ctrl Pts',(-24.585948047299,19.7560696421966,-62.0195638424871));
#55571=CARTESIAN_POINT('Ctrl Pts',(-24.4697262590945,19.724344659937,-62.0134763427692));
#55572=CARTESIAN_POINT('Ctrl Pts',(-24.3519515589681,19.6979390274756,-62.0073888430513));
#55573=CARTESIAN_POINT('Ctrl Pts',(-24.233153611916,19.6769935531812,-62.0013013433334));
#55574=CARTESIAN_POINT('Ctrl Pts',(-24.1189539922797,19.6568588180542,-61.99544947325));
#55575=CARTESIAN_POINT('Ctrl Pts',(-24.0038093117721,19.6417694851315,-61.9895976031666));
#55576=CARTESIAN_POINT('Ctrl Pts',(-23.8882019391522,19.6317988573478,-61.9837457330832));
#55577=CARTESIAN_POINT('Ctrl Pts',(-23.772612168806,19.6218297476828,-61.9778947540003));
#55578=CARTESIAN_POINT('Ctrl Pts',(-23.6565602581637,19.6169778290317,-61.9720437749174));
#55579=CARTESIAN_POINT('Ctrl Pts',(-23.5405338081249,19.6172645395422,-61.9661927958344));
#55580=CARTESIAN_POINT('Ctrl Pts',(-23.4244969261917,19.6175512758306,-61.9603412906921));
#55581=CARTESIAN_POINT('Ctrl Pts',(-23.3084859228187,19.6229775586966,-61.9544897855499));
#55582=CARTESIAN_POINT('Ctrl Pts',(-23.1929877951504,19.6335127001478,-61.9486382804076));
#55583=CARTESIAN_POINT('Ctrl Pts',(-23.0774513130683,19.6440513400901,-61.9427848321078));
#55584=CARTESIAN_POINT('Ctrl Pts',(-22.9624284568071,19.659702174551,-61.9369313838081));
#55585=CARTESIAN_POINT('Ctrl Pts',(-22.8483997929683,19.6803828009225,-61.9310779355084));
#55586=CARTESIAN_POINT('Ctrl Pts',(-22.7342414537779,19.7010869456569,-61.9252178305668));
#55587=CARTESIAN_POINT('Ctrl Pts',(-22.6210799706674,19.7268322253675,-61.9193577256253));
#55588=CARTESIAN_POINT('Ctrl Pts',(-22.509384526914,19.7574853629077,-61.9134976206838));
#55589=CARTESIAN_POINT('Ctrl Pts',(-22.3976138632701,19.7881591434174,-61.9076335693284));
#55590=CARTESIAN_POINT('Ctrl Pts',(-22.287311597317,19.8237472363157,-61.9017695179729));
#55591=CARTESIAN_POINT('Ctrl Pts',(-22.1789289326433,19.864067432342,-61.8959054666175));
#55592=CARTESIAN_POINT('Ctrl Pts',(-22.070386533557,19.9044470522886,-61.890032772821));
#55593=CARTESIAN_POINT('Ctrl Pts',(-21.9637697613652,19.9495725339506,-61.8841600790244));
#55594=CARTESIAN_POINT('Ctrl Pts',(-21.8595072237068,19.9992147533091,-61.8782873852279));
#55595=CARTESIAN_POINT('Ctrl Pts',(-21.8309618849919,20.012805962558,-61.8766795399044));
#55596=CARTESIAN_POINT('Ctrl Pts',(-21.8025928540155,20.0267354781966,-61.8750716945809));
#55597=CARTESIAN_POINT('Ctrl Pts',(-21.7744085517583,20.0409980298199,-61.8734638492574));
#55598=CARTESIAN_POINT('Ctrl Pts',(-21.6714716645523,20.0930888232805,-61.8675915522886));
#55599=CARTESIAN_POINT('Ctrl Pts',(-21.5706562406025,20.1497998911861,-61.8617192553199));
#55600=CARTESIAN_POINT('Ctrl Pts',(-21.472405827772,20.2109349255058,-61.8558469583512));
#55601=CARTESIAN_POINT('Ctrl Pts',(-21.3742827396737,20.2719907336763,-61.849982271413));
#55602=CARTESIAN_POINT('Ctrl Pts',(-21.2787184000945,20.337458890786,-61.8441175844748));
#55603=CARTESIAN_POINT('Ctrl Pts',(-21.1861337144921,20.407096280702,-61.8382528975366));
#55604=CARTESIAN_POINT('Ctrl Pts',(-21.093644246443,20.4766620529219,-61.8323942420617));
#55605=CARTESIAN_POINT('Ctrl Pts',(-21.0041286655255,20.5503882823135,-61.8265355865869));
#55606=CARTESIAN_POINT('Ctrl Pts',(-20.9179801394522,20.6279878186607,-61.8206769311121));
#55607=CARTESIAN_POINT('Ctrl Pts',(-20.828466576072,20.7086184612463,-61.8145894313942));
#55608=CARTESIAN_POINT('Ctrl Pts',(-20.7425888561999,20.7934309287559,-61.8085019316763));
#55609=CARTESIAN_POINT('Ctrl Pts',(-20.6607517506638,20.8820557180343,-61.8024144319584));
#55610=CARTESIAN_POINT('Ctrl Pts',(-20.5820823244967,20.9672500961961,-61.796562561875));
#55611=CARTESIAN_POINT('Ctrl Pts',(-20.5071468343922,21.0559668237066,-61.7907106917916));
#55612=CARTESIAN_POINT('Ctrl Pts',(-20.4362676921025,21.1478396989793,-61.7848588217081));
#55613=CARTESIAN_POINT('Ctrl Pts',(-20.3653993418067,21.2396985857713,-61.7790078426252));
#55614=CARTESIAN_POINT('Ctrl Pts',(-20.2985863637469,21.3347123376244,-61.7731568635422));
#55615=CARTESIAN_POINT('Ctrl Pts',(-20.2361103631534,21.4324823159484,-61.7673058844592));
#55616=CARTESIAN_POINT('Ctrl Pts',(-20.1736287453662,21.5302610847344,-61.7614543793169));
#55617=CARTESIAN_POINT('Ctrl Pts',(-20.1154851028063,21.6307962242594,-61.7556028741746));
#55618=CARTESIAN_POINT('Ctrl Pts',(-20.0619168597525,21.7336614274942,-61.7497513690323));
#55619=CARTESIAN_POINT('Ctrl Pts',(-20.0083308278512,21.8365607900236,-61.7438979207325));
#55620=CARTESIAN_POINT('Ctrl Pts',(-19.9593234075026,21.9417913883908,-61.7380444724327));
#55621=CARTESIAN_POINT('Ctrl Pts',(-19.9150850386307,22.0489043717478,-61.732191024133));
#55622=CARTESIAN_POINT('Ctrl Pts',(-19.8707963611272,22.156139165826,-61.7263309191914));
#55623=CARTESIAN_POINT('Ctrl Pts',(-19.8312877180315,22.2652602353222,-61.7204708142499));
#55624=CARTESIAN_POINT('Ctrl Pts',(-19.7967005944955,22.3758008065254,-61.7146107093083));
#55625=CARTESIAN_POINT('Ctrl Pts',(-19.7620901786965,22.4864158198849,-61.7087466579529));
#55626=CARTESIAN_POINT('Ctrl Pts',(-19.7324079875653,22.5984518398084,-61.7028826065974));
#55627=CARTESIAN_POINT('Ctrl Pts',(-19.7077446200612,22.7114307693167,-61.6970185552419));
#55628=CARTESIAN_POINT('Ctrl Pts',(-19.6830449036768,22.8245762072145,-61.6911458614454));
#55629=CARTESIAN_POINT('Ctrl Pts',(-19.6633788433503,22.9386669223457,-61.6852731676488));
#55630=CARTESIAN_POINT('Ctrl Pts',(-19.6487853537993,23.0532184686673,-61.6794004738522));
#55631=CARTESIAN_POINT('Ctrl Pts',(-19.6447899004797,23.0845807658353,-61.6777926285289));
#55632=CARTESIAN_POINT('Ctrl Pts',(-19.6411743718086,23.1159776012902,-61.6761847832057));
#55633=CARTESIAN_POINT('Ctrl Pts',(-19.6379388856029,23.1473990414423,-61.6745769378824));
#55634=CARTESIAN_POINT('Ctrl Pts',(-19.6261219927944,23.2621588539,-61.6687046409137));
#55635=CARTESIAN_POINT('Ctrl Pts',(-19.6193389552216,23.3776312979306,-61.662832343945));
#55636=CARTESIAN_POINT('Ctrl Pts',(-19.617664372068,23.4933370964622,-61.6569600469763));
#55637=CARTESIAN_POINT('Ctrl Pts',(-19.6159919590411,23.6088929494682,-61.6510953600381));
#55638=CARTESIAN_POINT('Ctrl Pts',(-19.6194148412559,23.7246811460681,-61.6452306730999));
#55639=CARTESIAN_POINT('Ctrl Pts',(-19.6279559982741,23.840216156862,-61.6393659861617));
#55640=CARTESIAN_POINT('Ctrl Pts',(-19.6364883712469,23.9556323471299,-61.6335073306869));
#55641=CARTESIAN_POINT('Ctrl Pts',(-19.6501285187102,24.070795459733,-61.6276486752121));
#55642=CARTESIAN_POINT('Ctrl Pts',(-19.6688473801853,24.1852194992131,-61.6217900197373));
#55643=CARTESIAN_POINT('Ctrl Pts',(-19.688297416877,24.3041130424587,-61.6157025200194));
#55644=CARTESIAN_POINT('Ctrl Pts',(-19.7132310205916,24.4222081432094,-61.6096150203014));
#55645=CARTESIAN_POINT('Ctrl Pts',(-19.7435561179166,24.5389645288567,-61.6035275205835));
#55646=CARTESIAN_POINT('Ctrl Pts',(-19.7727074177994,24.6512016100684,-61.5976756505001));
#55647=CARTESIAN_POINT('Ctrl Pts',(-19.8068404800227,24.7622012473678,-61.5918237804167));
#55648=CARTESIAN_POINT('Ctrl Pts',(-19.8458214902675,24.8714942428562,-61.5859719103333));
#55649=CARTESIAN_POINT('Ctrl Pts',(-19.8847965652991,24.9807705974923,-61.5801209312504));
#55650=CARTESIAN_POINT('Ctrl Pts',(-19.9286179818527,25.088340437734,-61.5742699521674));
#55651=CARTESIAN_POINT('Ctrl Pts',(-19.9771025781589,25.1937513633187,-61.5684189730844));
#55652=CARTESIAN_POINT('Ctrl Pts',(-20.025591533697,25.29917176636,-61.5625674679421));
#55653=CARTESIAN_POINT('Ctrl Pts',(-20.0787443296951,25.4024324932943,-61.5567159627998));
#55654=CARTESIAN_POINT('Ctrl Pts',(-20.1363306447845,25.5031033580705,-61.5508644576575));
#55655=CARTESIAN_POINT('Ctrl Pts',(-20.1939360830355,25.6038076534493,-61.5450110093578));
#55656=CARTESIAN_POINT('Ctrl Pts',(-20.2559777627562,25.7019200179063,-61.539157561058));
#55657=CARTESIAN_POINT('Ctrl Pts',(-20.3221809990495,25.7970376082266,-61.5333041127582));
#55658=CARTESIAN_POINT('Ctrl Pts',(-20.3884595227982,25.8922633679015,-61.5274440078167));
#55659=CARTESIAN_POINT('Ctrl Pts',(-20.458908812942,25.9844872162568,-61.5215839028751));
#55660=CARTESIAN_POINT('Ctrl Pts',(-20.5332126436486,26.0733378084817,-61.5157237979336));
#55661=CARTESIAN_POINT('Ctrl Pts',(-20.6075665133347,26.1622482360195,-61.5098597465782));
#55662=CARTESIAN_POINT('Ctrl Pts',(-20.6857798140403,26.2477805797459,-61.5039956952227));
#55663=CARTESIAN_POINT('Ctrl Pts',(-20.7674992873335,26.3296001855512,-61.4981316438673));
#55664=CARTESIAN_POINT('Ctrl Pts',(-20.8493391988177,26.4115403771226,-61.4922589500707));
#55665=CARTESIAN_POINT('Ctrl Pts',(-20.9346952923896,26.4897566318144,-61.4863862562741));
#55666=CARTESIAN_POINT('Ctrl Pts',(-21.0231810305196,26.5639543463983,-61.4805135624776));
#55667=CARTESIAN_POINT('Ctrl Pts',(-21.0474069454341,26.5842684394754,-61.4789057171542));
#55668=CARTESIAN_POINT('Ctrl Pts',(-21.0718672833677,26.6042815649795,-61.4772978718309));
#55669=CARTESIAN_POINT('Ctrl Pts',(-21.0965537507095,26.6239882542628,-61.4756900265075));
#55670=CARTESIAN_POINT('Ctrl Pts',(-21.186715574882,26.6959625480965,-61.4698177295388));
#55671=CARTESIAN_POINT('Ctrl Pts',(-21.2801979601086,26.7640869826368,-61.4639454325701));
#55672=CARTESIAN_POINT('Ctrl Pts',(-21.3766380065686,26.8280397267639,-61.4580731356014));
#55673=CARTESIAN_POINT('Ctrl Pts',(-21.4729530743875,26.8919095932136,-61.4522084486632));
#55674=CARTESIAN_POINT('Ctrl Pts',(-21.5722178398534,26.9516182938486,-61.446343761725));
#55675=CARTESIAN_POINT('Ctrl Pts',(-21.6740362403629,27.0068840463545,-61.4404790747868));
#55676=CARTESIAN_POINT('Ctrl Pts',(-21.7757499270213,27.0620929614936,-61.434620419312));
#55677=CARTESIAN_POINT('Ctrl Pts',(-21.8800116638402,27.1128678210478,-61.4287617638371));
#55678=CARTESIAN_POINT('Ctrl Pts',(-21.9863968662657,27.1589703729374,-61.4229031083623));
#55679=CARTESIAN_POINT('Ctrl Pts',(-22.0969375684009,27.2068737311105,-61.4168156086444));
#55680=CARTESIAN_POINT('Ctrl Pts',(-22.2097706279095,27.2497320803257,-61.4107281089265));
#55681=CARTESIAN_POINT('Ctrl Pts',(-22.3243917347984,27.2873308432411,-61.4046406092086));
#55682=CARTESIAN_POINT('Ctrl Pts',(-22.4345761877612,27.3234742660046,-61.3987887391252));
#55683=CARTESIAN_POINT('Ctrl Pts',(-22.5464124121354,27.3547575576321,-61.3929368690418));
#55684=CARTESIAN_POINT('Ctrl Pts',(-22.6594333315443,27.3810396770005,-61.3870849989584));
#55685=CARTESIAN_POINT('Ctrl Pts',(-22.7724370424906,27.4073177946773,-61.3812340198754));
#55686=CARTESIAN_POINT('Ctrl Pts',(-22.8866246872882,27.4285961605441,-61.3753830407925));
#55687=CARTESIAN_POINT('Ctrl Pts',(-23.0015166473045,27.44478433015,-61.3695320617095));
#55688=CARTESIAN_POINT('Ctrl Pts',(-23.1164189372138,27.4609739552281,-61.3636805565672));
#55689=CARTESIAN_POINT('Ctrl Pts',(-23.2320252588615,27.4720724165851,-61.3578290514249));
#55690=CARTESIAN_POINT('Ctrl Pts',(-23.3478491910413,27.4780409536554,-61.3519775462826));
#55691=CARTESIAN_POINT('Ctrl Pts',(-23.4637115858275,27.4840114727469,-61.3461240979828));
#55692=CARTESIAN_POINT('Ctrl Pts',(-23.5797913222211,27.4848486589147,-61.3402706496831));
#55693=CARTESIAN_POINT('Ctrl Pts',(-23.6956010026349,27.4805658553359,-61.3344172013833));
#55694=CARTESIAN_POINT('Ctrl Pts',(-23.8115423838029,27.4762781812794,-61.3285570964417));
#55695=CARTESIAN_POINT('Ctrl Pts',(-23.9272126826588,27.4668589111484,-61.3226969915002));
#55696=CARTESIAN_POINT('Ctrl Pts',(-24.0421285471146,27.4523733634284,-61.3168368865587));
#55697=CARTESIAN_POINT('Ctrl Pts',(-24.1571218002129,27.4378780605987,-61.3109728352032));
#55698=CARTESIAN_POINT('Ctrl Pts',(-24.2713592008013,27.4183097561906,-61.3051087838478));
#55699=CARTESIAN_POINT('Ctrl Pts',(-24.3843682476043,27.3937847577165,-61.2992447324923));
#55700=CARTESIAN_POINT('Ctrl Pts',(-24.4975438471834,27.3692236142903,-61.2933720386958));
#55701=CARTESIAN_POINT('Ctrl Pts',(-24.6094870816644,27.3396913021259,-61.2874993448992));
#55702=CARTESIAN_POINT('Ctrl Pts',(-24.7197411564874,27.3053537761987,-61.2816266511026));
#55703=CARTESIAN_POINT('Ctrl Pts',(-24.7499268778493,27.2959527359962,-61.2800188057793));
#55704=CARTESIAN_POINT('Ctrl Pts',(-24.7799861057219,27.2861917860426,-61.2784109604559));
#55705=CARTESIAN_POINT('Ctrl Pts',(-24.8099097561921,27.2760749478555,-61.2768031151325));
#55706=CARTESIAN_POINT('Ctrl Pts',(-24.9191992253931,27.2391254494459,-61.2709308181638));
#55707=CARTESIAN_POINT('Ctrl Pts',(-25.0270446473952,27.1973012951529,-61.2650585211951));
#55708=CARTESIAN_POINT('Ctrl Pts',(-25.1329790975397,27.1507338353211,-61.2591862242264));
#55709=CARTESIAN_POINT('Ctrl Pts',(-25.2387762650499,27.1042267232189,-61.2533215372882));
#55710=CARTESIAN_POINT('Ctrl Pts',(-25.3426670105679,27.0529886944684,-61.24745685035));
#55711=CARTESIAN_POINT('Ctrl Pts',(-25.4442001772773,26.9972006478964,-61.2415921634118));
#55712=CARTESIAN_POINT('Ctrl Pts',(-25.545628923481,26.9414699758379,-61.235733507937));
#55713=CARTESIAN_POINT('Ctrl Pts',(-25.6447045534566,26.881198791411,-61.2298748524622));
#55714=CARTESIAN_POINT('Ctrl Pts',(-25.7409971157814,26.8166155193753,-61.2240161969873));
#55715=CARTESIAN_POINT('Ctrl Pts',(-25.8410509504038,26.7495095678497,-61.2179286972694));
#55716=CARTESIAN_POINT('Ctrl Pts',(-25.9380994506838,26.6777479763894,-61.2118411975515));
#55717=CARTESIAN_POINT('Ctrl Pts',(-26.0316894881728,26.601639041303,-61.2057536978336));
#55718=CARTESIAN_POINT('Ctrl Pts',(-26.1216569240439,26.5284760645554,-61.1999018277502));
#55719=CARTESIAN_POINT('Ctrl Pts',(-26.2084283025172,26.4512963178911,-61.1940499576668));
#55720=CARTESIAN_POINT('Ctrl Pts',(-26.2916324887472,26.3704165217962,-61.1881980875835));
#55721=CARTESIAN_POINT('Ctrl Pts',(-26.3748240063832,26.2895490403857,-61.1823471085005));
#55722=CARTESIAN_POINT('Ctrl Pts',(-26.4544491153716,26.2049829177538,-61.1764961294175));
#55723=CARTESIAN_POINT('Ctrl Pts',(-26.5301724690748,26.1170727760435,-61.1706451503346));
#55724=CARTESIAN_POINT('Ctrl Pts',(-26.6059026310362,26.0291547303655,-61.1647936451923));
#55725=CARTESIAN_POINT('Ctrl Pts',(-26.677730070539,25.9378923811526,-61.15894214005));
#55726=CARTESIAN_POINT('Ctrl Pts',(-26.7453592463859,25.843674010998,-61.1530906349077));
#55727=CARTESIAN_POINT('Ctrl Pts',(-26.81301088041,25.7494243529736,-61.1472371866079));
#55728=CARTESIAN_POINT('Ctrl Pts',(-26.8764612376695,25.6522170577456,-61.1413837383082));
#55729=CARTESIAN_POINT('Ctrl Pts',(-26.9354580849452,25.5524693936347,-61.1355302900084));
#55730=CARTESIAN_POINT('Ctrl Pts',(-26.9945220244471,25.4526082947699,-61.1296701850669));
#55731=CARTESIAN_POINT('Ctrl Pts',(-27.0491221345907,25.3502014167806,-61.1238100801253));
#55732=CARTESIAN_POINT('Ctrl Pts',(-27.0990520966194,25.2456907192984,-61.1179499751838));
#55733=CARTESIAN_POINT('Ctrl Pts',(-27.1490156833525,25.1411096404028,-61.1120859238284));
#55734=CARTESIAN_POINT('Ctrl Pts',(-27.1943026984173,25.0344223004926,-61.1062218724729));
#55735=CARTESIAN_POINT('Ctrl Pts',(-27.234755586305,24.92608909196,-61.1003578211175));
#55736=CARTESIAN_POINT('Ctrl Pts',(-27.2752680936743,24.8175962219032,-61.0944851273209));
#55737=CARTESIAN_POINT('Ctrl Pts',(-27.3109321277976,24.7074530338344,-61.0886124335244));
#55738=CARTESIAN_POINT('Ctrl Pts',(-27.3416403925553,24.5961335423809,-61.0827397397278));
#55739=CARTESIAN_POINT('Ctrl Pts',(-27.3500478017595,24.5656561277684,-61.0811318944044));
#55740=CARTESIAN_POINT('Ctrl Pts',(-27.358084037758,24.5350905877725,-61.0795240490811));
#55741=CARTESIAN_POINT('Ctrl Pts',(-27.365747573681,24.5044467386427,-61.0779162037578));
#55742=CARTESIAN_POINT('Ctrl Pts',(-27.4044761963103,24.3495842729633,-61.0697907593937));
#55743=CARTESIAN_POINT('Ctrl Pts',(-27.4337921536769,24.1922805254554,-61.0616653150297));
#55744=CARTESIAN_POINT('Ctrl Pts',(-27.4534487225508,24.0335210861051,-61.0535398706656));
#55745=CARTESIAN_POINT('Ctrl Pts',(-27.4717796892775,23.8854680856582,-61.0459623910336));
#55746=CARTESIAN_POINT('Ctrl Pts',(-27.4817105553438,23.736148950333,-61.0383849114016));
#55747=CARTESIAN_POINT('Ctrl Pts',(-27.4830865394795,23.586386549012,-61.0308074317696));
#55748=CARTESIAN_POINT('Ctrl Pts',(-27.4831860436438,23.575556494944,-61.0302594670376));
#55749=CARTESIAN_POINT('Ctrl Pts',(-27.4832408301729,23.564724134297,-61.0297115023055));
#55750=CARTESIAN_POINT('Ctrl Pts',(-27.4832508498222,23.5538897837606,-61.0291635375734));
#55751=CARTESIAN_POINT('',(-27.4768264258044,23.5495998111571,-59.7791635220347));
#55752=CARTESIAN_POINT('Ctrl Pts',(-27.4827541867016,23.5538890172514,-61.0291635220347));
#55753=CARTESIAN_POINT('Ctrl Pts',(-27.4736971142189,22.5645208266935,-60.9791187788174));
#55754=CARTESIAN_POINT('Ctrl Pts',(-26.5929390169561,20.2501455696673,-60.8627783984751));
#55755=CARTESIAN_POINT('Ctrl Pts',(-22.7010557676678,18.9764558934434,-60.680142381008));
#55756=CARTESIAN_POINT('Ctrl Pts',(-19.2432138286812,21.7923650373258,-60.481255469633));
#55757=CARTESIAN_POINT('Ctrl Pts',(-19.7431752811021,26.223623744252,-60.2823685582583));
#55758=CARTESIAN_POINT('Ctrl Pts',(-23.7415179398966,28.1982809713375,-60.0834816468832));
#55759=CARTESIAN_POINT('Ctrl Pts',(-26.9653676070822,26.2614956795997,-59.9157466348087));
#55760=CARTESIAN_POINT('Ctrl Pts',(-27.4757968990708,24.247026390915,-59.8143072598592));
#55761=CARTESIAN_POINT('Ctrl Pts',(-27.4768264258044,23.5495998111571,-59.7791635220347));
#55762=CARTESIAN_POINT('',(-27.4834398043345,23.546843952154,-58.5291636146978));
#55763=CARTESIAN_POINT('Ctrl Pts',(-27.4768264258044,23.5495998111571,-59.7791635220347));
#55764=CARTESIAN_POINT('Ctrl Pts',(-27.4777390126582,22.9313911649828,-59.7480116227343));
#55765=CARTESIAN_POINT('Ctrl Pts',(-27.0484773771044,20.9987458094278,-59.6505640863089));
#55766=CARTESIAN_POINT('Ctrl Pts',(-24.0207930075597,18.9221489791923,-59.4868209127587));
#55767=CARTESIAN_POINT('Ctrl Pts',(-19.9108984363416,20.6526927651409,-59.2879340013836));
#55768=CARTESIAN_POINT('Ctrl Pts',(-19.1452617124101,25.0458483039971,-59.0890470900089));
#55769=CARTESIAN_POINT('Ctrl Pts',(-22.4274380697694,28.0646781337172,-58.8901601786339));
#55770=CARTESIAN_POINT('Ctrl Pts',(-26.4754744607769,27.0047585962735,-58.7035326345686));
#55771=CARTESIAN_POINT('Ctrl Pts',(-27.475398742621,24.6134662246994,-58.5832007276283));
#55772=CARTESIAN_POINT('Ctrl Pts',(-27.4851571966465,23.5468591049139,-58.5291644578129));
#55773=CARTESIAN_POINT('',(-27.4849330916743,23.5524945914181,-57.2791629100328));
#55774=CARTESIAN_POINT('Ctrl Pts',(-27.483251053208,23.54684228678,-58.5291635220347));
#55775=CARTESIAN_POINT('Ctrl Pts',(-27.4831007264043,23.3734720123943,-58.5203759322785));
#55776=CARTESIAN_POINT('Ctrl Pts',(-27.4714837675545,23.2005800536994,-58.5115883425223));
#55777=CARTESIAN_POINT('Ctrl Pts',(-27.4486073494167,23.0293699008261,-58.502800752766));
#55778=CARTESIAN_POINT('Ctrl Pts',(-27.4395702071008,22.9617347269926,-58.4993292871387));
#55779=CARTESIAN_POINT('Ctrl Pts',(-27.4287763948297,22.8943616140389,-58.4958578215115));
#55780=CARTESIAN_POINT('Ctrl Pts',(-27.4162404617435,22.827323541604,-58.4923863558842));
#55781=CARTESIAN_POINT('Ctrl Pts',(-27.3950348011478,22.7139226003837,-58.4865140589155));
#55782=CARTESIAN_POINT('Ctrl Pts',(-27.3687998039024,22.6012655107326,-58.4806417619468));
#55783=CARTESIAN_POINT('Ctrl Pts',(-27.3375998206115,22.4898330330376,-58.4747694649781));
#55784=CARTESIAN_POINT('Ctrl Pts',(-27.306440270021,22.378544962984,-58.4689047780399));
#55785=CARTESIAN_POINT('Ctrl Pts',(-27.2703286391819,22.268478743313,-58.4630400911017));
#55786=CARTESIAN_POINT('Ctrl Pts',(-27.2293805527643,22.1601064945539,-58.4571754041635));
#55787=CARTESIAN_POINT('Ctrl Pts',(-27.1884745788902,22.0518456998686,-58.4513167486887));
#55788=CARTESIAN_POINT('Ctrl Pts',(-27.1427421881976,21.9452757952577,-58.4454580932138));
#55789=CARTESIAN_POINT('Ctrl Pts',(-27.092349042018,21.8408545933686,-58.439599437739));
#55790=CARTESIAN_POINT('Ctrl Pts',(-27.0399874951629,21.7323546073606,-58.4335119380211));
#55791=CARTESIAN_POINT('Ctrl Pts',(-26.9825937862766,21.626175044375,-58.4274244383032));
#55792=CARTESIAN_POINT('Ctrl Pts',(-26.9204093929195,21.5228079009493,-58.4213369385853));
#55793=CARTESIAN_POINT('Ctrl Pts',(-26.8606319788736,21.4234418028384,-58.4154850685019));
#55794=CARTESIAN_POINT('Ctrl Pts',(-26.7964280846312,21.3266748385302,-58.4096331984185));
#55795=CARTESIAN_POINT('Ctrl Pts',(-26.7280590640968,21.2329190117581,-58.4037813283351));
#55796=CARTESIAN_POINT('Ctrl Pts',(-26.6597004533674,21.1391774601632,-58.3979303492521));
#55797=CARTESIAN_POINT('Ctrl Pts',(-26.587178220795,21.0484464684288,-58.3920793701691));
#55798=CARTESIAN_POINT('Ctrl Pts',(-26.5107962801063,20.9611079405718,-58.3862283910862));
#55799=CARTESIAN_POINT('Ctrl Pts',(-26.434407471946,20.8737615601406,-58.3803768859439));
#55800=CARTESIAN_POINT('Ctrl Pts',(-26.3541585379674,20.7898085611189,-58.3745253808016));
#55801=CARTESIAN_POINT('Ctrl Pts',(-26.2703923178979,20.7095961738234,-58.3686738756593));
#55802=CARTESIAN_POINT('Ctrl Pts',(-26.1865982808901,20.6293571497402,-58.3628204273595));
#55803=CARTESIAN_POINT('Ctrl Pts',(-26.0992849336816,20.5528614931237,-58.3569669790597));
#55804=CARTESIAN_POINT('Ctrl Pts',(-26.0088299065595,20.4804176351891,-58.3511135307599));
#55805=CARTESIAN_POINT('Ctrl Pts',(-25.9182720124298,20.4078913928573,-58.3452534258184));
#55806=CARTESIAN_POINT('Ctrl Pts',(-25.8245656300914,20.3394264047519,-58.3393933208768));
#55807=CARTESIAN_POINT('Ctrl Pts',(-25.7281192954062,20.2752891182316,-58.3335332159353));
#55808=CARTESIAN_POINT('Ctrl Pts',(-25.631608010151,20.2111086392631,-58.3276691645798));
#55809=CARTESIAN_POINT('Ctrl Pts',(-25.5323534515609,20.1512618780335,-58.3218051132244));
#55810=CARTESIAN_POINT('Ctrl Pts',(-25.4307892655792,20.0959695970594,-58.3159410618689));
#55811=CARTESIAN_POINT('Ctrl Pts',(-25.3290753942615,20.0405958263006,-58.3100683680724));
#55812=CARTESIAN_POINT('Ctrl Pts',(-25.2250454720223,19.9897901131692,-58.3041956742758));
#55813=CARTESIAN_POINT('Ctrl Pts',(-25.1191537027079,19.943725377271,-58.2983229804792));
#55814=CARTESIAN_POINT('Ctrl Pts',(-25.0901623076226,19.931113623151,-58.2967151351559));
#55815=CARTESIAN_POINT('Ctrl Pts',(-25.0610314420914,19.918856951594,-58.2951072898326));
#55816=CARTESIAN_POINT('Ctrl Pts',(-25.0317706099032,19.9069582553641,-58.2934994445092));
#55817=CARTESIAN_POINT('Ctrl Pts',(-24.9249019368617,19.8635009172803,-58.2876271475405));
#55818=CARTESIAN_POINT('Ctrl Pts',(-24.8159405089581,19.8246769278107,-58.2817548505718));
#55819=CARTESIAN_POINT('Ctrl Pts',(-24.7053255822017,19.7906920190822,-58.2758825536031));
#55820=CARTESIAN_POINT('Ctrl Pts',(-24.5948540036055,19.7567511520964,-58.2700178666649));
#55821=CARTESIAN_POINT('Ctrl Pts',(-24.4827335789287,19.7276370152407,-58.2641531797267));
#55822=CARTESIAN_POINT('Ctrl Pts',(-24.36942401113,19.703507532701,-58.2582884927885));
#55823=CARTESIAN_POINT('Ctrl Pts',(-24.2562309751285,19.6794028658236,-58.2524298373136));
#55824=CARTESIAN_POINT('Ctrl Pts',(-24.14185163042,19.6602727421615,-58.2465711818388));
#55825=CARTESIAN_POINT('Ctrl Pts',(-24.0267606894386,19.646225255201,-58.240712526364));
#55826=CARTESIAN_POINT('Ctrl Pts',(-23.9071741949318,19.6316290610269,-58.2346250266461));
#55827=CARTESIAN_POINT('Ctrl Pts',(-23.7868198143401,19.6225207962139,-58.2285375269282));
#55828=CARTESIAN_POINT('Ctrl Pts',(-23.6662420014635,19.6189632466247,-58.2224500272103));
#55829=CARTESIAN_POINT('Ctrl Pts',(-23.5503314094976,19.6155433995648,-58.2165981571269));
#55830=CARTESIAN_POINT('Ctrl Pts',(-23.4342148122107,19.6172525665684,-58.2107462870435));
#55831=CARTESIAN_POINT('Ctrl Pts',(-23.3183801081215,19.6240935716944,-58.2048944169601));
#55832=CARTESIAN_POINT('Ctrl Pts',(-23.2025630409193,19.6309335352152,-58.1990434378771));
#55833=CARTESIAN_POINT('Ctrl Pts',(-23.087028194125,19.6429037588822,-58.1931924587941));
#55834=CARTESIAN_POINT('Ctrl Pts',(-22.9722611482489,19.659954990289,-58.1873414797112));
#55835=CARTESIAN_POINT('Ctrl Pts',(-22.8574837837109,19.6770077547657,-58.1814899745689));
#55836=CARTESIAN_POINT('Ctrl Pts',(-22.7434747662406,19.6991423743668,-58.1756384694266));
#55837=CARTESIAN_POINT('Ctrl Pts',(-22.630711545936,19.726258104984,-58.1697869642843));
#55838=CARTESIAN_POINT('Ctrl Pts',(-22.5179108794207,19.753382840145,-58.1639335159845));
#55839=CARTESIAN_POINT('Ctrl Pts',(-22.4063572344046,19.7854918788342,-58.1580800676848));
#55840=CARTESIAN_POINT('Ctrl Pts',(-22.2965142244232,19.822434234502,-58.152226619385));
#55841=CARTESIAN_POINT('Ctrl Pts',(-22.1865462990875,19.85941860165,-58.1463665144434));
#55842=CARTESIAN_POINT('Ctrl Pts',(-22.0782932837225,19.9012471248324,-58.1405064095019));
#55843=CARTESIAN_POINT('Ctrl Pts',(-21.972200175914,19.9477201220667,-58.1346463045604));
#55844=CARTESIAN_POINT('Ctrl Pts',(-21.8660356210376,19.994224415956,-58.1287822532049));
#55845=CARTESIAN_POINT('Ctrl Pts',(-21.7620342400739,20.0453792298865,-58.1229182018495));
#55846=CARTESIAN_POINT('Ctrl Pts',(-21.6606161682483,20.1009390617494,-58.117054150494));
#55847=CARTESIAN_POINT('Ctrl Pts',(-21.5590486264297,20.1565807777136,-58.1111814566974));
#55848=CARTESIAN_POINT('Ctrl Pts',(-21.4600723444297,20.2166402549786,-58.1053087629009));
#55849=CARTESIAN_POINT('Ctrl Pts',(-21.3640783188479,20.2808288346054,-58.0994360691043));
#55850=CARTESIAN_POINT('Ctrl Pts',(-21.3377967604277,20.2984025939633,-58.097828223781));
#55851=CARTESIAN_POINT('Ctrl Pts',(-21.311738549237,20.3162856293256,-58.0962203784577));
#55852=CARTESIAN_POINT('Ctrl Pts',(-21.2859112562073,20.334471508657,-58.0946125331343));
#55853=CARTESIAN_POINT('Ctrl Pts',(-21.191582820276,20.4008913828341,-58.0887402361656));
#55854=CARTESIAN_POINT('Ctrl Pts',(-21.1000212755521,20.471576448137,-58.0828679391969));
#55855=CARTESIAN_POINT('Ctrl Pts',(-21.0116371444203,20.5462683580514,-58.0769956422282));
#55856=CARTESIAN_POINT('Ctrl Pts',(-20.9233675521031,20.6208634731825,-58.07113095529));
#55857=CARTESIAN_POINT('Ctrl Pts',(-20.8382674976224,20.6994548424408,-58.0652662683518));
#55858=CARTESIAN_POINT('Ctrl Pts',(-20.7567183341826,20.7817410747316,-58.0594015814136));
#55859=CARTESIAN_POINT('Ctrl Pts',(-20.6752530389524,20.8639426807837,-58.0535429259388));
#55860=CARTESIAN_POINT('Ctrl Pts',(-20.597331660246,20.949831299749,-58.047684270464));
#55861=CARTESIAN_POINT('Ctrl Pts',(-20.5233017411223,21.0390659772033,-58.0418256149892));
#55862=CARTESIAN_POINT('Ctrl Pts',(-20.4463801481528,21.1317862397559,-58.0357381152713));
#55863=CARTESIAN_POINT('Ctrl Pts',(-20.3736605672507,21.2281189962251,-58.0296506155534));
#55864=CARTESIAN_POINT('Ctrl Pts',(-20.3054901215756,21.3276401269143,-58.0235631158355));
#55865=CARTESIAN_POINT('Ctrl Pts',(-20.2399583581088,21.4233090803983,-58.0177112457521));
#55866=CARTESIAN_POINT('Ctrl Pts',(-20.1786303656202,21.5219237991508,-58.0118593756687));
#55867=CARTESIAN_POINT('Ctrl Pts',(-20.121772249871,21.6230753324856,-58.0060075055853));
#55868=CARTESIAN_POINT('Ctrl Pts',(-20.0649227912869,21.7242114645798,-58.0001565265023));
#55869=CARTESIAN_POINT('Ctrl Pts',(-20.0125420587352,21.8278832830057,-57.9943055474193));
#55870=CARTESIAN_POINT('Ctrl Pts',(-19.9648510921911,21.9336556377194,-57.9884545683363));
#55871=CARTESIAN_POINT('Ctrl Pts',(-19.9171558377701,22.0394375023857,-57.982603063194));
#55872=CARTESIAN_POINT('Ctrl Pts',(-19.8741513574927,22.1473199019024,-57.9767515580518));
#55873=CARTESIAN_POINT('Ctrl Pts',(-19.8360109756684,22.2568466930297,-57.9709000529095));
#55874=CARTESIAN_POINT('Ctrl Pts',(-19.7978579282537,22.3664098556201,-57.9650466046097));
#55875=CARTESIAN_POINT('Ctrl Pts',(-19.7645723270104,22.4776181054569,-57.9591931563099));
#55876=CARTESIAN_POINT('Ctrl Pts',(-19.736277747191,22.5899997820634,-57.9533397080102));
#55877=CARTESIAN_POINT('Ctrl Pts',(-19.7079509902902,22.7025092610394,-57.9474796030686));
#55878=CARTESIAN_POINT('Ctrl Pts',(-19.6846266846769,22.8161944291788,-57.9416194981271));
#55879=CARTESIAN_POINT('Ctrl Pts',(-19.666377374609,22.9305729659697,-57.9357593931855));
#55880=CARTESIAN_POINT('Ctrl Pts',(-19.6481157747729,23.0450285295464,-57.9298953418301));
#55881=CARTESIAN_POINT('Ctrl Pts',(-19.6349360226784,23.1601779818479,-57.9240312904746));
#55882=CARTESIAN_POINT('Ctrl Pts',(-19.6268586741821,23.2755351517625,-57.9181672391192));
#55883=CARTESIAN_POINT('Ctrl Pts',(-19.6187694212866,23.3910623351181,-57.9122945453226));
#55884=CARTESIAN_POINT('Ctrl Pts',(-19.6157975908789,23.5067974353769,-57.9064218515261));
#55885=CARTESIAN_POINT('Ctrl Pts',(-19.6179116795881,23.6222554681455,-57.9005491577295));
#55886=CARTESIAN_POINT('Ctrl Pts',(-19.6184904817123,23.6538659461412,-57.8989413124061));
#55887=CARTESIAN_POINT('Ctrl Pts',(-19.619450211574,23.6854556951569,-57.8973334670828));
#55888=CARTESIAN_POINT('Ctrl Pts',(-19.6207895502036,23.717014868853,-57.8957256217594));
#55889=CARTESIAN_POINT('Ctrl Pts',(-19.6256811862707,23.8322777223989,-57.8898533247907));
#55890=CARTESIAN_POINT('Ctrl Pts',(-19.6356568211889,23.9475182605663,-57.883981027822));
#55891=CARTESIAN_POINT('Ctrl Pts',(-19.6507210084532,24.0622514567418,-57.8781087308533));
#55892=CARTESIAN_POINT('Ctrl Pts',(-19.6657656737272,24.176835967807,-57.8722440439151));
#55893=CARTESIAN_POINT('Ctrl Pts',(-19.6858857242154,24.2909140382802,-57.8663793569769));
#55894=CARTESIAN_POINT('Ctrl Pts',(-19.7110337321068,24.4040019146483,-57.8605146700387));
#55895=CARTESIAN_POINT('Ctrl Pts',(-19.7361558768464,24.5169734872149,-57.8546560145639));
#55896=CARTESIAN_POINT('Ctrl Pts',(-19.7662956045298,24.6289564901325,-57.8487973590891));
#55897=CARTESIAN_POINT('Ctrl Pts',(-19.8013539262362,24.7394742292742,-57.8429387036143));
#55898=CARTESIAN_POINT('Ctrl Pts',(-19.8377816568674,24.8543088886495,-57.8368512038963));
#55899=CARTESIAN_POINT('Ctrl Pts',(-19.8795200049003,24.9675610308765,-57.8307637041784));
#55900=CARTESIAN_POINT('Ctrl Pts',(-19.9263997861015,25.0787093607413,-57.8246762044605));
#55901=CARTESIAN_POINT('Ctrl Pts',(-19.9714649855825,25.1855554579069,-57.8188243343771));
#55902=CARTESIAN_POINT('Ctrl Pts',(-20.0212808232329,25.2904571630241,-57.8129724642937));
#55903=CARTESIAN_POINT('Ctrl Pts',(-20.0756470834238,25.3929695416689,-57.8071205942103));
#55904=CARTESIAN_POINT('Ctrl Pts',(-20.1300050658573,25.4954663118718,-57.8012696151274));
#55905=CARTESIAN_POINT('Ctrl Pts',(-20.1889118996094,25.5955741138439,-57.7954186360444));
#55906=CARTESIAN_POINT('Ctrl Pts',(-20.2521209671241,25.6928717658994,-57.7895676569614));
#55907=CARTESIAN_POINT('Ctrl Pts',(-20.3153357177422,25.7901781659503,-57.7837161518191));
#55908=CARTESIAN_POINT('Ctrl Pts',(-20.3828532458539,25.8846735671458,-57.7778646466768));
#55909=CARTESIAN_POINT('Ctrl Pts',(-20.4543834796354,25.9759655840778,-57.7720131415346));
#55910=CARTESIAN_POINT('Ctrl Pts',(-20.5259374670503,26.0672879171014,-57.7661596932348));
#55911=CARTESIAN_POINT('Ctrl Pts',(-20.6015065549688,26.1554044253906,-57.760306244935));
#55912=CARTESIAN_POINT('Ctrl Pts',(-20.6807607251806,26.2399561905294,-57.7544527966352));
#55913=CARTESIAN_POINT('Ctrl Pts',(-20.7601050245937,26.3246041093852,-57.7485926916937));
#55914=CARTESIAN_POINT('Ctrl Pts',(-20.8431424880157,26.4056788918743,-57.7427325867522));
#55915=CARTESIAN_POINT('Ctrl Pts',(-20.9295065443544,26.4828587906117,-57.7368724818106));
#55916=CARTESIAN_POINT('Ctrl Pts',(-21.0159287614796,26.5600906651804,-57.7310084304552));
#55917=CARTESIAN_POINT('Ctrl Pts',(-21.1056817129704,26.6334221722514,-57.7251443790997));
#55918=CARTESIAN_POINT('Ctrl Pts',(-21.1983674862254,26.7025732217415,-57.7192803277443));
#55919=CARTESIAN_POINT('Ctrl Pts',(-21.2911898598083,26.7718261860747,-57.7134076339477));
#55920=CARTESIAN_POINT('Ctrl Pts',(-21.386953341168,26.8368861649078,-57.7075349401512));
#55921=CARTESIAN_POINT('Ctrl Pts',(-21.4852328758897,26.8975175079309,-57.7016622463546));
#55922=CARTESIAN_POINT('Ctrl Pts',(-21.5121401684809,26.9141173554123,-57.7000544010312));
#55923=CARTESIAN_POINT('Ctrl Pts',(-21.5392359290243,26.9303855171045,-57.6984465557079));
#55924=CARTESIAN_POINT('Ctrl Pts',(-21.5665111606702,26.9463177803147,-57.6968387103845));
#55925=CARTESIAN_POINT('Ctrl Pts',(-21.6661278699325,27.004506823499,-57.6909664134158));
#55926=CARTESIAN_POINT('Ctrl Pts',(-21.7684739217973,27.0584065507413,-57.6850941164471));
#55927=CARTESIAN_POINT('Ctrl Pts',(-21.8731437165943,27.1077509536635,-57.6792218194784));
#55928=CARTESIAN_POINT('Ctrl Pts',(-21.97767786765,27.1570314101584,-57.6733571325402));
#55929=CARTESIAN_POINT('Ctrl Pts',(-22.0845294026075,27.201768107307,-57.667492445602));
#55930=CARTESIAN_POINT('Ctrl Pts',(-22.1932656947774,27.2417394576408,-57.6616277586638));
#55931=CARTESIAN_POINT('Ctrl Pts',(-22.3018901584778,27.281669699943,-57.655769103189));
#55932=CARTESIAN_POINT('Ctrl Pts',(-22.4123951382376,27.3168442017246,-57.6499104477142));
#55933=CARTESIAN_POINT('Ctrl Pts',(-22.5243260755816,27.3470885706414,-57.6440517922393));
#55934=CARTESIAN_POINT('Ctrl Pts',(-22.6406291339257,27.378514311247,-57.6379642925214));
#55935=CARTESIAN_POINT('Ctrl Pts',(-22.7584714078796,27.4046167227234,-57.6318767928035));
#55936=CARTESIAN_POINT('Ctrl Pts',(-22.8773228717832,27.4252563604422,-57.6257892930856));
#55937=CARTESIAN_POINT('Ctrl Pts',(-22.9915739367877,27.4450970970494,-57.6199374230022));
#55938=CARTESIAN_POINT('Ctrl Pts',(-23.1067570734629,27.4598900157265,-57.6140855529188));
#55939=CARTESIAN_POINT('Ctrl Pts',(-23.2223897259773,27.469563055323,-57.6082336828354));
#55940=CARTESIAN_POINT('Ctrl Pts',(-23.338004772369,27.4792346221112,-57.6023827037524));
#55941=CARTESIAN_POINT('Ctrl Pts',(-23.4540687866825,27.4837878253591,-57.5965317246695));
#55942=CARTESIAN_POINT('Ctrl Pts',(-23.5700941144552,27.4832024819979,-57.5906807455865));
#55943=CARTESIAN_POINT('Ctrl Pts',(-23.6861298740214,27.4826170860086,-57.5848292404442));
#55944=CARTESIAN_POINT('Ctrl Pts',(-23.8021265267299,27.4768922270731,-57.5789777353019));
#55945=CARTESIAN_POINT('Ctrl Pts',(-23.9175971560356,27.4660598465359,-57.5731262301596));
#55946=CARTESIAN_POINT('Ctrl Pts',(-24.0331061306234,27.4552238688009,-57.5672727818599));
#55947=CARTESIAN_POINT('Ctrl Pts',(-24.1480883231084,27.4392770354725,-57.5614193335601));
#55948=CARTESIAN_POINT('Ctrl Pts',(-24.2620633805721,27.4183029857886,-57.5555658852604));
#55949=CARTESIAN_POINT('Ctrl Pts',(-24.3761680524256,27.3973050840557,-57.5497057803188));
#55950=CARTESIAN_POINT('Ctrl Pts',(-24.489262896414,27.371268629795,-57.5438456753773));
#55951=CARTESIAN_POINT('Ctrl Pts',(-24.6008790738485,27.3403281073155,-57.5379855704357));
#55952=CARTESIAN_POINT('Ctrl Pts',(-24.7125704177926,27.3093667483306,-57.5321215190803));
#55953=CARTESIAN_POINT('Ctrl Pts',(-24.822780720244,27.2734948726593,-57.5262574677248));
#55954=CARTESIAN_POINT('Ctrl Pts',(-24.9310592480865,27.2328958502856,-57.5203934163694));
#55955=CARTESIAN_POINT('Ctrl Pts',(-25.0394973568647,27.1922369930572,-57.5145207225728));
#55956=CARTESIAN_POINT('Ctrl Pts',(-25.1459976300264,27.1468372460935,-57.5086480287763));
#55957=CARTESIAN_POINT('Ctrl Pts',(-25.2501320510816,27.0969268358229,-57.5027753349797));
#55958=CARTESIAN_POINT('Ctrl Pts',(-25.2786423136107,27.0832622003899,-57.5011674896564));
#55959=CARTESIAN_POINT('Ctrl Pts',(-25.3069753982381,27.0692597134763,-57.499559644333));
#55960=CARTESIAN_POINT('Ctrl Pts',(-25.335122897576,27.0549246671438,-57.4979517990097));
#55961=CARTESIAN_POINT('Ctrl Pts',(-25.4379253703254,27.0025691028975,-57.492079502041));
#55962=CARTESIAN_POINT('Ctrl Pts',(-25.5385944949873,26.9455987398224,-57.4862072050723));
#55963=CARTESIAN_POINT('Ctrl Pts',(-25.6366872304336,26.8842110269212,-57.4803349081036));
#55964=CARTESIAN_POINT('Ctrl Pts',(-25.7346528454852,26.8229028676205,-57.4744702211654));
#55965=CARTESIAN_POINT('Ctrl Pts',(-25.8300483638023,26.7571889598113,-57.4686055342272));
#55966=CARTESIAN_POINT('Ctrl Pts',(-25.9224535070639,26.6873135021656,-57.462740847289));
#55967=CARTESIAN_POINT('Ctrl Pts',(-26.01476361742,26.617509907054,-57.4568821918142));
#55968=CARTESIAN_POINT('Ctrl Pts',(-26.1040891421339,26.5435535228683,-57.4510235363393));
#55969=CARTESIAN_POINT('Ctrl Pts',(-26.1900376538747,26.4657325108253,-57.4451648808645));
#55970=CARTESIAN_POINT('Ctrl Pts',(-26.2793433901867,26.3848717415081,-57.4390773811466));
#55971=CARTESIAN_POINT('Ctrl Pts',(-26.3650025316752,26.2998385192065,-57.4329898814287));
#55972=CARTESIAN_POINT('Ctrl Pts',(-26.4466112598961,26.2110033876686,-57.4269023817108));
#55973=CARTESIAN_POINT('Ctrl Pts',(-26.5250611485779,26.1256068089924,-57.4210505116274));
#55974=CARTESIAN_POINT('Ctrl Pts',(-26.5997680475929,26.0366975031978,-57.415198641544));
#55975=CARTESIAN_POINT('Ctrl Pts',(-26.6704104888022,25.9446425004954,-57.4093467714606));
#55976=CARTESIAN_POINT('Ctrl Pts',(-26.7410421740574,25.8526015140042,-57.4034957923776));
#55977=CARTESIAN_POINT('Ctrl Pts',(-26.8076103803839,25.757416110791,-57.3976448132947));
#55978=CARTESIAN_POINT('Ctrl Pts',(-26.869834529517,25.6594856529331,-57.3917938342117));
#55979=CARTESIAN_POINT('Ctrl Pts',(-26.9320642731998,25.5615463901846,-57.3859423290694));
#55980=CARTESIAN_POINT('Ctrl Pts',(-26.9899489615603,25.4608619310919,-57.3800908239272));
#55981=CARTESIAN_POINT('Ctrl Pts',(-27.0432522683531,25.3578591923647,-57.3742393187849));
#55982=CARTESIAN_POINT('Ctrl Pts',(-27.0965732760138,25.2548222486705,-57.3683858704851));
#55983=CARTESIAN_POINT('Ctrl Pts',(-27.145309687054,25.149465861485,-57.3625324221853));
#55984=CARTESIAN_POINT('Ctrl Pts',(-27.1892722174519,25.0422393703318,-57.3566789738856));
#55985=CARTESIAN_POINT('Ctrl Pts',(-27.2332847427933,24.9348909393742,-57.3508188689441));
#55986=CARTESIAN_POINT('Ctrl Pts',(-27.2725123945841,24.8256685423021,-57.3449587640025));
#55987=CARTESIAN_POINT('Ctrl Pts',(-27.3068148895434,24.7150393154407,-57.339098659061));
#55988=CARTESIAN_POINT('Ctrl Pts',(-27.3411404850861,24.604335586719,-57.3332346077055));
#55989=CARTESIAN_POINT('Ctrl Pts',(-27.3705342148381,24.4922235406138,-57.3273705563501));
#55990=CARTESIAN_POINT('Ctrl Pts',(-27.3949067106861,24.3791815057082,-57.3215065049947));
#55991=CARTESIAN_POINT('Ctrl Pts',(-27.4193151267278,24.2659728694086,-57.3156338111981));
#55992=CARTESIAN_POINT('Ctrl Pts',(-27.4386874703901,24.1518319148441,-57.3097611174015));
#55993=CARTESIAN_POINT('Ctrl Pts',(-27.4529860739721,24.0372431866136,-57.303888423605));
#55994=CARTESIAN_POINT('Ctrl Pts',(-27.4569007924465,24.0058707096587,-57.3022805782816));
#55995=CARTESIAN_POINT('Ctrl Pts',(-27.4604354986348,23.9744646723974,-57.3006727329582));
#55996=CARTESIAN_POINT('Ctrl Pts',(-27.4635901002877,23.9430350086899,-57.2990648876349));
#55997=CARTESIAN_POINT('Ctrl Pts',(-27.4766056310531,23.8133597596587,-57.2924310991015));
#55998=CARTESIAN_POINT('Ctrl Pts',(-27.4831771127117,23.6830269945391,-57.2857973105681));
#55999=CARTESIAN_POINT('Ctrl Pts',(-27.4832518862965,23.5525056845392,-57.2791635220347));
#56000=CARTESIAN_POINT('',(-27.4814477670606,23.552581764037,-56.0291640430588));
#56001=CARTESIAN_POINT('Ctrl Pts',(-27.4881430614576,23.5524734110292,-57.2791617415215));
#56002=CARTESIAN_POINT('Ctrl Pts',(-27.4801041554848,22.3771595256381,-57.2195004864343));
#56003=CARTESIAN_POINT('Ctrl Pts',(-26.2965486380378,19.8818213561216,-57.0935435942221));
#56004=CARTESIAN_POINT('Ctrl Pts',(-22.0489891170354,19.1471900756399,-56.9012910648851));
#56005=CARTESIAN_POINT('Ctrl Pts',(-19.0343856930495,22.433248714451,-56.7024041535101));
#56006=CARTESIAN_POINT('Ctrl Pts',(-20.1694810114101,26.7457391550027,-56.5035172421352));
#56007=CARTESIAN_POINT('Ctrl Pts',(-24.411218714757,28.1218483213208,-56.3046303307603));
#56008=CARTESIAN_POINT('Ctrl Pts',(-27.1544722338234,25.8760995970628,-56.1465129185815));
#56009=CARTESIAN_POINT('Ctrl Pts',(-27.4808162851497,24.0587493601289,-56.0546911435275));
#56010=CARTESIAN_POINT('Ctrl Pts',(-27.4781149091143,23.5525988839457,-56.0291650055986));
#56011=CARTESIAN_POINT('',(-27.4822168486201,23.5471344304972,-54.7791631113927));
#56012=CARTESIAN_POINT('Ctrl Pts',(-27.4832518474532,23.5525724970079,-56.0291635220347));
#56013=CARTESIAN_POINT('Ctrl Pts',(-27.4833210457297,23.4352617887352,-56.0232550255369));
#56014=CARTESIAN_POINT('Ctrl Pts',(-27.4781373133555,23.3179395204581,-56.0173465290391));
#56015=CARTESIAN_POINT('Ctrl Pts',(-27.4677241201152,23.2011030595281,-56.0114380325413));
#56016=CARTESIAN_POINT('Ctrl Pts',(-27.4573091591171,23.0842467642809,-56.0055285330091));
#56017=CARTESIAN_POINT('Ctrl Pts',(-27.4416630057699,22.9678768410211,-55.9996190334769));
#56018=CARTESIAN_POINT('Ctrl Pts',(-27.420861003246,22.8524853355955,-55.9937095339447));
#56019=CARTESIAN_POINT('Ctrl Pts',(-27.4000508088788,22.7370483889136,-55.9877977072474));
#56020=CARTESIAN_POINT('Ctrl Pts',(-27.3740807956718,22.6225910223746,-55.9818858805501));
#56021=CARTESIAN_POINT('Ctrl Pts',(-27.3430772746285,22.5095943412275,-55.9759740538528));
#56022=CARTESIAN_POINT('Ctrl Pts',(-27.3120322330754,22.3964463327587,-55.9700543099239));
#56023=CARTESIAN_POINT('Ctrl Pts',(-27.2759403254324,22.2847633054023,-55.9641345659949));
#56024=CARTESIAN_POINT('Ctrl Pts',(-27.2349777000081,22.1750109405568,-55.958214822066));
#56025=CARTESIAN_POINT('Ctrl Pts',(-27.1939868338899,22.0651829095912,-55.9522909969124));
#56026=CARTESIAN_POINT('Ctrl Pts',(-27.1481187161183,21.9572885630109,-55.9463671717588));
#56027=CARTESIAN_POINT('Ctrl Pts',(-27.0975968319451,21.8517716176191,-55.9404433466052));
#56028=CARTESIAN_POINT('Ctrl Pts',(-27.0469818102325,21.746060150807,-55.9345086008277));
#56029=CARTESIAN_POINT('Ctrl Pts',(-26.9916960677777,21.6427351980163,-55.9285738550501));
#56030=CARTESIAN_POINT('Ctrl Pts',(-26.932008429644,21.5422146718217,-55.9226391092726));
#56031=CARTESIAN_POINT('Ctrl Pts',(-26.8790982052221,21.4531080533279,-55.9173782421853));
#56032=CARTESIAN_POINT('Ctrl Pts',(-26.8227297304176,21.3662048814533,-55.9121173750979));
#56033=CARTESIAN_POINT('Ctrl Pts',(-26.7631168605512,21.2817746710224,-55.9068565080106));
#56034=CARTESIAN_POINT('Ctrl Pts',(-26.6965756480093,21.187531790419,-55.9009842110419));
#56035=CARTESIAN_POINT('Ctrl Pts',(-26.6257728086476,21.0960612877013,-55.8951119140732));
#56036=CARTESIAN_POINT('Ctrl Pts',(-26.5509672170767,21.0077733524422,-55.8892396171045));
#56037=CARTESIAN_POINT('Ctrl Pts',(-26.4762585676116,20.9195998313355,-55.8833749301663));
#56038=CARTESIAN_POINT('Ctrl Pts',(-26.3975577462774,20.8346009883091,-55.8775102432281));
#56039=CARTESIAN_POINT('Ctrl Pts',(-26.3151666346911,20.7531577883848,-55.8716455562899));
#56040=CARTESIAN_POINT('Ctrl Pts',(-26.2328602572054,20.6717983476934,-55.8657869008151));
#56041=CARTESIAN_POINT('Ctrl Pts',(-26.1468714306049,20.5939875654901,-55.8599282453403));
#56042=CARTESIAN_POINT('Ctrl Pts',(-26.0575415562922,20.5200725457643,-55.8540695898655));
#56043=CARTESIAN_POINT('Ctrl Pts',(-25.9647223784078,20.4432703402642,-55.8479820901476));
#56044=CARTESIAN_POINT('Ctrl Pts',(-25.8682961172614,20.3706747923508,-55.8418945904297));
#56045=CARTESIAN_POINT('Ctrl Pts',(-25.7686873389186,20.3026324790872,-55.8358070907118));
#56046=CARTESIAN_POINT('Ctrl Pts',(-25.67293413037,20.2372238883941,-55.8299552206284));
#56047=CARTESIAN_POINT('Ctrl Pts',(-25.5742405689188,20.1760228561691,-55.824103350545));
#56048=CARTESIAN_POINT('Ctrl Pts',(-25.4730159473699,20.1192949616652,-55.8182514804616));
#56049=CARTESIAN_POINT('Ctrl Pts',(-25.3718067381901,20.0625757044991,-55.8124005013786));
#56050=CARTESIAN_POINT('Ctrl Pts',(-25.2680675956813,20.0103284328963,-55.8065495222956));
#56051=CARTESIAN_POINT('Ctrl Pts',(-25.1622339539886,19.9627736266443,-55.8006985432127));
#56052=CARTESIAN_POINT('Ctrl Pts',(-25.0563907968331,19.9152145447578,-55.7948470380704));
#56053=CARTESIAN_POINT('Ctrl Pts',(-24.9484531432285,19.8723489363555,-55.7889955329281));
#56054=CARTESIAN_POINT('Ctrl Pts',(-24.8388773590915,19.8343495385827,-55.7831440277858));
#56055=CARTESIAN_POINT('Ctrl Pts',(-24.7292651872215,19.7963375220369,-55.777290579486));
#56056=CARTESIAN_POINT('Ctrl Pts',(-24.6180141934921,19.7631950647314,-55.7714371311862));
#56057=CARTESIAN_POINT('Ctrl Pts',(-24.5055961970215,19.7350451348258,-55.7655836828864));
#56058=CARTESIAN_POINT('Ctrl Pts',(-24.3930503568783,19.7068631923375,-55.7597235779449));
#56059=CARTESIAN_POINT('Ctrl Pts',(-24.2793352663113,19.6836852100147,-55.7538634730033));
#56060=CARTESIAN_POINT('Ctrl Pts',(-24.1649333387917,19.6655831113463,-55.7480033680618));
#56061=CARTESIAN_POINT('Ctrl Pts',(-24.0504543687342,19.6474688220474,-55.7421393167063));
#56062=CARTESIAN_POINT('Ctrl Pts',(-23.9352880504695,19.6344372692628,-55.7362752653509));
#56063=CARTESIAN_POINT('Ctrl Pts',(-23.8199205811606,19.6265083831676,-55.7304112139954));
#56064=CARTESIAN_POINT('Ctrl Pts',(-23.7043830832316,19.618567811477,-55.7245385201989));
#56065=CARTESIAN_POINT('Ctrl Pts',(-23.5886442542966,19.6157449256096,-55.7186658264023));
#56066=CARTESIAN_POINT('Ctrl Pts',(-23.4731890378049,19.6180075980832,-55.7127931326057));
#56067=CARTESIAN_POINT('Ctrl Pts',(-23.4415793308591,19.6186270799566,-55.7111852872824));
#56068=CARTESIAN_POINT('Ctrl Pts',(-23.4099908431004,19.6196274625754,-55.7095774419591));
#56069=CARTESIAN_POINT('Ctrl Pts',(-23.3784334191629,19.6210074142996,-55.7079695966357));
#56070=CARTESIAN_POINT('Ctrl Pts',(-23.2631769562199,19.6260473806506,-55.702097299667));
#56071=CARTESIAN_POINT('Ctrl Pts',(-23.1479493513484,19.6361713129244,-55.6962250026983));
#56072=CARTESIAN_POINT('Ctrl Pts',(-23.0332356366199,19.6513831404209,-55.6903527057296));
#56073=CARTESIAN_POINT('Ctrl Pts',(-22.9186705817551,19.6665752545971,-55.6844880187914));
#56074=CARTESIAN_POINT('Ctrl Pts',(-22.8046184986894,19.6868420980349,-55.6786233318532));
#56075=CARTESIAN_POINT('Ctrl Pts',(-22.6915630794992,19.7121356204096,-55.6727586449149));
#56076=CARTESIAN_POINT('Ctrl Pts',(-22.5786239307304,19.7374031299798,-55.6668999894401));
#56077=CARTESIAN_POINT('Ctrl Pts',(-22.4666798080314,19.7676869461267,-55.6610413339653));
#56078=CARTESIAN_POINT('Ctrl Pts',(-22.3562072777432,19.8028874665428,-55.6551826784905));
#56079=CARTESIAN_POINT('Ctrl Pts',(-22.2414195931189,19.8394629502906,-55.6490951787726));
#56080=CARTESIAN_POINT('Ctrl Pts',(-22.1282212586844,19.8813470104659,-55.6430076790547));
#56081=CARTESIAN_POINT('Ctrl Pts',(-22.0171333514949,19.928369792109,-55.6369201793368));
#56082=CARTESIAN_POINT('Ctrl Pts',(-21.9103453382162,19.9735724568954,-55.6310683092534));
#56083=CARTESIAN_POINT('Ctrl Pts',(-21.8055078290779,20.0235232536357,-55.62521643917));
#56084=CARTESIAN_POINT('Ctrl Pts',(-21.7030655004737,20.0780213942711,-55.6193645690865));
#56085=CARTESIAN_POINT('Ctrl Pts',(-21.6006387696455,20.1325112370689,-55.6135135900036));
#56086=CARTESIAN_POINT('Ctrl Pts',(-21.500606859088,20.1915468530021,-55.6076626109206));
#56087=CARTESIAN_POINT('Ctrl Pts',(-21.4033906327606,20.2548810826908,-55.6018116318376));
#56088=CARTESIAN_POINT('Ctrl Pts',(-21.3061656657588,20.3182210067362,-55.5959601266953));
#56089=CARTESIAN_POINT('Ctrl Pts',(-21.2117572326247,20.385860087175,-55.590108621553));
#56090=CARTESIAN_POINT('Ctrl Pts',(-21.1205573451418,20.4575077474541,-55.5842571164107));
#56091=CARTESIAN_POINT('Ctrl Pts',(-21.0293271721614,20.5291792003617,-55.5784036681109));
#56092=CARTESIAN_POINT('Ctrl Pts',(-20.9413079883829,20.6048616248008,-55.5725502198111));
#56093=CARTESIAN_POINT('Ctrl Pts',(-20.8568582872175,20.6842245409342,-55.5666967715114));
#56094=CARTESIAN_POINT('Ctrl Pts',(-20.7723125484041,20.7636777099364,-55.5608366665698));
#56095=CARTESIAN_POINT('Ctrl Pts',(-20.6913446958137,20.8468194415406,-55.5549765616283));
#56096=CARTESIAN_POINT('Ctrl Pts',(-20.6142760048163,20.9332827508939,-55.5491164566867));
#56097=CARTESIAN_POINT('Ctrl Pts',(-20.5371554128789,21.0198042878746,-55.5432524053313));
#56098=CARTESIAN_POINT('Ctrl Pts',(-20.4639394716058,21.1096515369929,-55.5373883539758));
#56099=CARTESIAN_POINT('Ctrl Pts',(-20.3949077587654,21.2024262255227,-55.5315243026204));
#56100=CARTESIAN_POINT('Ctrl Pts',(-20.3257743069605,21.2953376454236,-55.5256516088238));
#56101=CARTESIAN_POINT('Ctrl Pts',(-20.2608376221606,21.3911847746194,-55.5197789150272));
#56102=CARTESIAN_POINT('Ctrl Pts',(-20.2003328074686,21.4895422557835,-55.5139062212307));
#56103=CARTESIAN_POINT('Ctrl Pts',(-20.183767601328,21.5164708888062,-55.5122983759074));
#56104=CARTESIAN_POINT('Ctrl Pts',(-20.1675343232456,21.5435875627712,-55.5106905305841));
#56105=CARTESIAN_POINT('Ctrl Pts',(-20.1516371743323,21.5708832754148,-55.5090826852607));
#56106=CARTESIAN_POINT('Ctrl Pts',(-20.0935763782963,21.6705747869621,-55.503210388292));
#56107=CARTESIAN_POINT('Ctrl Pts',(-20.0398084071022,21.7729901188356,-55.4973380913233));
#56108=CARTESIAN_POINT('Ctrl Pts',(-19.9905987469325,21.8777233293686,-55.4914657943546));
#56109=CARTESIAN_POINT('Ctrl Pts',(-19.9414528585742,21.9823208139786,-55.4856011074164));
#56110=CARTESIAN_POINT('Ctrl Pts',(-19.8968537080926,22.0892298331064,-55.4797364204782));
#56111=CARTESIAN_POINT('Ctrl Pts',(-19.8570223260157,22.1980174752548,-55.47387173354));
#56112=CARTESIAN_POINT('Ctrl Pts',(-19.8172319080216,22.3066932361237,-55.4680130780652));
#56113=CARTESIAN_POINT('Ctrl Pts',(-19.7821996466882,22.4172433912263,-55.4621544225904));
#56114=CARTESIAN_POINT('Ctrl Pts',(-19.7520993492335,22.5292131580345,-55.4562957671155));
#56115=CARTESIAN_POINT('Ctrl Pts',(-19.7208233076483,22.6455565625555,-55.4502082673976));
#56116=CARTESIAN_POINT('Ctrl Pts',(-19.694872571635,22.763432330701,-55.4441207676797));
#56117=CARTESIAN_POINT('Ctrl Pts',(-19.6743859036046,22.8823102577951,-55.4380332679618));
#56118=CARTESIAN_POINT('Ctrl Pts',(-19.6546922156685,22.9965867616761,-55.4321813978784));
#56119=CARTESIAN_POINT('Ctrl Pts',(-19.6400475409863,23.1117888403065,-55.426329527795));
#56120=CARTESIAN_POINT('Ctrl Pts',(-19.6305233196369,23.2274338455175,-55.4204776577117));
#56121=CARTESIAN_POINT('Ctrl Pts',(-19.6210005484369,23.3430612427248,-55.4146266786287));
#56122=CARTESIAN_POINT('Ctrl Pts',(-19.6165967143256,23.4591310205462,-55.4087756995457));
#56123=CARTESIAN_POINT('Ctrl Pts',(-19.6173313727817,23.5751554989486,-55.4029247204628));
#56124=CARTESIAN_POINT('Ctrl Pts',(-19.6180660972906,23.6911904090681,-55.3970732153205));
#56125=CARTESIAN_POINT('Ctrl Pts',(-19.6239402301624,23.8071795982729,-55.3912217101782));
#56126=CARTESIAN_POINT('Ctrl Pts',(-19.6349212034552,23.9226361915271,-55.3853702050359));
#56127=CARTESIAN_POINT('Ctrl Pts',(-19.6459058232902,24.0381311254019,-55.3795167567362));
#56128=CARTESIAN_POINT('Ctrl Pts',(-19.6620006165586,24.1530927003363,-55.3736633084365));
#56129=CARTESIAN_POINT('Ctrl Pts',(-19.6831213259151,24.2670406714466,-55.3678098601367));
#56130=CARTESIAN_POINT('Ctrl Pts',(-19.7042660541046,24.3811182261442,-55.3619497551952));
#56131=CARTESIAN_POINT('Ctrl Pts',(-19.7304480310795,24.4941794695873,-55.3560896502537));
#56132=CARTESIAN_POINT('Ctrl Pts',(-19.7615321692833,24.6057557365463,-55.3502295453121));
#56133=CARTESIAN_POINT('Ctrl Pts',(-19.7926372407087,24.7174071431378,-55.3443654939567));
#56134=CARTESIAN_POINT('Ctrl Pts',(-19.8286509187688,24.8275711900096,-55.3385014426012));
#56135=CARTESIAN_POINT('Ctrl Pts',(-19.8693892535732,24.9357973804018,-55.3326373912458));
#56136=CARTESIAN_POINT('Ctrl Pts',(-19.910187628551,25.0441830745949,-55.3267646974492));
#56137=CARTESIAN_POINT('Ctrl Pts',(-19.9557243954944,25.1506248336195,-55.3208920036526));
#56138=CARTESIAN_POINT('Ctrl Pts',(-20.0057687773416,25.2546949376237,-55.3150193098561));
#56139=CARTESIAN_POINT('Ctrl Pts',(-20.0194700919515,25.2831875912205,-55.3134114645327));
#56140=CARTESIAN_POINT('Ctrl Pts',(-20.033509029748,25.3115026322737,-55.3118036192093));
#56141=CARTESIAN_POINT('Ctrl Pts',(-20.0478802878541,25.339631660213,-55.310195773886));
#56142=CARTESIAN_POINT('Ctrl Pts',(-20.1003681075384,25.4423666702912,-55.3043234769172));
#56143=CARTESIAN_POINT('Ctrl Pts',(-20.157467976777,25.5429623951609,-55.2984511799485));
#56144=CARTESIAN_POINT('Ctrl Pts',(-20.2189818765709,25.6409760481627,-55.2925788829798));
#56145=CARTESIAN_POINT('Ctrl Pts',(-20.280416059236,25.7388626832542,-55.2867141960416));
#56146=CARTESIAN_POINT('Ctrl Pts',(-20.3462526792466,25.8341735538834,-55.2808495091034));
#56147=CARTESIAN_POINT('Ctrl Pts',(-20.4162469972672,25.9264886963422,-55.2749848221652));
#56148=CARTESIAN_POINT('Ctrl Pts',(-20.4861693305134,26.0187088984558,-55.2691261666904));
#56149=CARTESIAN_POINT('Ctrl Pts',(-20.560240608465,26.1079391730819,-55.2632675112156));
#56150=CARTESIAN_POINT('Ctrl Pts',(-20.6381721651203,26.1937874640556,-55.2574088557408));
#56151=CARTESIAN_POINT('Ctrl Pts',(-20.71914779702,26.2829890648891,-55.2513213560229));
#56152=CARTESIAN_POINT('Ctrl Pts',(-20.8042911855645,26.3685387042961,-55.245233856305));
#56153=CARTESIAN_POINT('Ctrl Pts',(-20.8932312676302,26.4500330410279,-55.2391463565871));
#56154=CARTESIAN_POINT('Ctrl Pts',(-20.9787287345005,26.5283729659867,-55.2332944865037));
#56155=CARTESIAN_POINT('Ctrl Pts',(-21.0677341086437,26.6029653837714,-55.2274426164202));
#56156=CARTESIAN_POINT('Ctrl Pts',(-21.1598799464485,26.6734892988487,-55.2215907463368));
#56157=CARTESIAN_POINT('Ctrl Pts',(-21.2520117542115,26.7440024760186,-55.2157397672539));
#56158=CARTESIAN_POINT('Ctrl Pts',(-21.3472827467111,26.8104481310046,-55.2098887881709));
#56159=CARTESIAN_POINT('Ctrl Pts',(-21.4452932011183,26.8725461997226,-55.2040378090879));
#56160=CARTESIAN_POINT('Ctrl Pts',(-21.5433124676084,26.9346498516544,-55.1981863039456));
#56161=CARTESIAN_POINT('Ctrl Pts',(-21.644071336421,26.9924049190076,-55.1923347988034));
#56162=CARTESIAN_POINT('Ctrl Pts',(-21.7471425870662,27.0455756251412,-55.1864832936611));
#56163=CARTESIAN_POINT('Ctrl Pts',(-21.8502480654299,27.0987639881087,-55.1806298453613));
#56164=CARTESIAN_POINT('Ctrl Pts',(-21.9556670853445,27.1473647733088,-55.1747763970616));
#56165=CARTESIAN_POINT('Ctrl Pts',(-22.0629500640649,27.1911892751414,-55.1689229487618));
#56166=CARTESIAN_POINT('Ctrl Pts',(-22.1703550468282,27.2350636149489,-55.1630628438203));
#56167=CARTESIAN_POINT('Ctrl Pts',(-22.279627836394,27.2741506735195,-55.1572027388788));
#56168=CARTESIAN_POINT('Ctrl Pts',(-22.3903011162899,27.3083107688563,-55.1513426339372));
#56169=CARTESIAN_POINT('Ctrl Pts',(-22.501048927713,27.3424938688792,-55.1454785825818));
#56170=CARTESIAN_POINT('Ctrl Pts',(-22.6131987084253,27.3717432948005,-55.1396145312263));
#56171=CARTESIAN_POINT('Ctrl Pts',(-22.7262720152301,27.3959702941525,-55.1337504798709));
#56172=CARTESIAN_POINT('Ctrl Pts',(-22.8395119695179,27.4202329992656,-55.1278777860744));
#56173=CARTESIAN_POINT('Ctrl Pts',(-22.9536777602647,27.4394584363482,-55.1220050922778));
#56174=CARTESIAN_POINT('Ctrl Pts',(-23.0682847947976,27.4536095613023,-55.1161323984812));
#56175=CARTESIAN_POINT('Ctrl Pts',(-23.0996622837125,27.4574839025954,-55.1145245531578));
#56176=CARTESIAN_POINT('Ctrl Pts',(-23.1310728438597,27.4609781887276,-55.1129167078344));
#56177=CARTESIAN_POINT('Ctrl Pts',(-23.1625065412686,27.4640923402337,-55.111308862511));
#56178=CARTESIAN_POINT('Ctrl Pts',(-23.2773111206166,27.4754660850732,-55.1054365655423));
#56179=CARTESIAN_POINT('Ctrl Pts',(-23.392808891728,27.4818032608947,-55.0995642685736));
#56180=CARTESIAN_POINT('Ctrl Pts',(-23.5085202930935,27.4830311194438,-55.0936919716049));
#56181=CARTESIAN_POINT('Ctrl Pts',(-23.6240817416724,27.4842573867857,-55.0878272846667));
#56182=CARTESIAN_POINT('Ctrl Pts',(-23.7398558604101,27.4803874998374,-55.0819625977285));
#56183=CARTESIAN_POINT('Ctrl Pts',(-23.8553570348068,27.4714003537203,-55.0760979107903));
#56184=CARTESIAN_POINT('Ctrl Pts',(-23.9707394234761,27.4624224503204,-55.0702392553155));
#56185=CARTESIAN_POINT('Ctrl Pts',(-24.0858490164839,27.4483377875688,-55.0643805998407));
#56186=CARTESIAN_POINT('Ctrl Pts',(-24.2001999341894,27.4291773020384,-55.0585219443659));
#56187=CARTESIAN_POINT('Ctrl Pts',(-24.3190174994595,27.4092683910668,-55.052434444648));
#56188=CARTESIAN_POINT('Ctrl Pts',(-24.4370154574585,27.3838790365336,-55.0463469449301));
#56189=CARTESIAN_POINT('Ctrl Pts',(-24.5536538950772,27.3531033970268,-55.0402594452122));
#56190=CARTESIAN_POINT('Ctrl Pts',(-24.66577759369,27.3235189941566,-55.0344075751288));
#56191=CARTESIAN_POINT('Ctrl Pts',(-24.7766446242322,27.2889576435455,-55.0285557050453));
#56192=CARTESIAN_POINT('Ctrl Pts',(-24.8857863089272,27.2495549699749,-55.0227038349619));
#56193=CARTESIAN_POINT('Ctrl Pts',(-24.9949113758078,27.2101582958199,-55.016852855879));
#56194=CARTESIAN_POINT('Ctrl Pts',(-25.1023112304589,27.1659219047011,-55.0110018767961));
#56195=CARTESIAN_POINT('Ctrl Pts',(-25.2075341831328,27.117030703631,-55.0051508977131));
#56196=CARTESIAN_POINT('Ctrl Pts',(-25.3127665963632,27.0681351067712,-54.9992993925708));
#56197=CARTESIAN_POINT('Ctrl Pts',(-25.4158213436214,27.0145840421973,-54.9934478874285));
#56198=CARTESIAN_POINT('Ctrl Pts',(-25.5162691312773,26.9566094904059,-54.9875963822862));
#56199=CARTESIAN_POINT('Ctrl Pts',(-25.616750275457,26.8986156865278,-54.9817429339864));
#56200=CARTESIAN_POINT('Ctrl Pts',(-25.7146223807757,26.8361956810611,-54.9758894856866));
#56201=CARTESIAN_POINT('Ctrl Pts',(-25.8094836675129,26.7696257121359,-54.9700360373868));
#56202=CARTESIAN_POINT('Ctrl Pts',(-25.9044528321315,26.7029800387009,-54.9641759324453));
#56203=CARTESIAN_POINT('Ctrl Pts',(-25.996404005482,26.6321752196087,-54.9583158275038));
#56204=CARTESIAN_POINT('Ctrl Pts',(-26.0849670663925,26.5575289120073,-54.9524557225622));
#56205=CARTESIAN_POINT('Ctrl Pts',(-26.1735897689815,26.4828323347897,-54.9465916712068));
#56206=CARTESIAN_POINT('Ctrl Pts',(-26.2588195126049,26.4042893972812,-54.9407276198514));
#56207=CARTESIAN_POINT('Ctrl Pts',(-26.3403230094922,26.3222546472995,-54.9348635684959));
#56208=CARTESIAN_POINT('Ctrl Pts',(-26.4219466262642,26.240098994472,-54.9289908746994));
#56209=CARTESIAN_POINT('Ctrl Pts',(-26.4998327587808,26.1544415629824,-54.9231181809028));
#56210=CARTESIAN_POINT('Ctrl Pts',(-26.5736882983376,26.0656700248713,-54.9172454871063));
#56211=CARTESIAN_POINT('Ctrl Pts',(-26.5939087096164,26.0413658627024,-54.9156376417829));
#56212=CARTESIAN_POINT('Ctrl Pts',(-26.6138272505147,26.0168284412247,-54.9140297964595));
#56213=CARTESIAN_POINT('Ctrl Pts',(-26.633438484445,25.9920660751001,-54.9124219511362));
#56214=CARTESIAN_POINT('Ctrl Pts',(-26.7049732138191,25.9017418677765,-54.9065571095616));
#56215=CARTESIAN_POINT('Ctrl Pts',(-26.7726603804216,25.8081136964325,-54.9006922679871));
#56216=CARTESIAN_POINT('Ctrl Pts',(-26.8361786611447,25.7115434588474,-54.8948274264125));
#56217=CARTESIAN_POINT('Ctrl Pts',(-26.8996168611287,25.6150949722905,-54.8889699789431));
#56218=CARTESIAN_POINT('Ctrl Pts',(-26.9588963977614,25.5157121346701,-54.8831125314737));
#56219=CARTESIAN_POINT('Ctrl Pts',(-27.0137358333513,25.4137901404218,-54.8772550840044));
#56220=CARTESIAN_POINT('Ctrl Pts',(-27.0685194668807,25.3119718572574,-54.8714035968013));
#56221=CARTESIAN_POINT('Ctrl Pts',(-27.1188717875628,25.2076199165718,-54.8655521095982));
#56222=CARTESIAN_POINT('Ctrl Pts',(-27.1645547795137,25.1011581579034,-54.8597006223951));
#56223=CARTESIAN_POINT('Ctrl Pts',(-27.2102023940815,24.9947788443254,-54.8538536666443));
#56224=CARTESIAN_POINT('Ctrl Pts',(-27.2511877090005,24.8862933411769,-54.8480067108936));
#56225=CARTESIAN_POINT('Ctrl Pts',(-27.2873191081256,24.7761491029104,-54.8421597551429));
#56226=CARTESIAN_POINT('Ctrl Pts',(-27.3234340270074,24.6660551036019,-54.836315466304));
#56227=CARTESIAN_POINT('Ctrl Pts',(-27.3546993026387,24.5543042658531,-54.8304711774651));
#56228=CARTESIAN_POINT('Ctrl Pts',(-27.3809720672344,24.4413624239244,-54.8246268886261));
#56229=CARTESIAN_POINT('Ctrl Pts',(-27.4072375689592,24.3284518037582,-54.8187842153886));
#56230=CARTESIAN_POINT('Ctrl Pts',(-27.4285132143907,24.2143512380285,-54.812941542151));
#56231=CARTESIAN_POINT('Ctrl Pts',(-27.4447066747234,24.0995392763389,-54.8070988689135));
#56232=CARTESIAN_POINT('Ctrl Pts',(-27.4609036343248,23.9847025047637,-54.8012549331241));
#56233=CARTESIAN_POINT('Ctrl Pts',(-27.4720161551831,23.8691544399423,-54.7954109973347));
#56234=CARTESIAN_POINT('Ctrl Pts',(-27.4780035216107,23.7533809669516,-54.7895670615453));
#56235=CARTESIAN_POINT('Ctrl Pts',(-27.481556481205,23.6846798983596,-54.7860992150418));
#56236=CARTESIAN_POINT('Ctrl Pts',(-27.4833056850997,23.6158995597262,-54.7826313685382));
#56237=CARTESIAN_POINT('Ctrl Pts',(-27.4832513014648,23.5471417467537,-54.7791635220347));
#56238=CARTESIAN_POINT('',(-27.4893929762737,23.5491656528098,-53.5291635220347));
#56239=CARTESIAN_POINT('Ctrl Pts',(-27.4796534495588,23.5471163006375,-54.7791620938121));
#56240=CARTESIAN_POINT('Ctrl Pts',(-27.4828378583424,23.1137759715362,-54.7572864091285));
#56241=CARTESIAN_POINT('Ctrl Pts',(-27.216596050397,21.3709791532061,-54.6691150873199));
#56242=CARTESIAN_POINT('Ctrl Pts',(-24.6614438543076,19.0329519354699,-54.5146481283863));
#56243=CARTESIAN_POINT('Ctrl Pts',(-20.3504177643223,20.1735961539112,-54.3157612170115));
#56244=CARTESIAN_POINT('Ctrl Pts',(-18.9797685243006,24.4171012902892,-54.1168743056365));
#56245=CARTESIAN_POINT('Ctrl Pts',(-21.809006573937,27.8640459141707,-53.9179873942616));
#56246=CARTESIAN_POINT('Ctrl Pts',(-26.1718623003577,27.3547361893404,-53.7220837997278));
#56247=CARTESIAN_POINT('Ctrl Pts',(-27.4848291776058,24.7953569349182,-53.5924758423187));
#56248=CARTESIAN_POINT('Ctrl Pts',(-27.4893929762737,23.5491656528098,-53.5291635220347));
#56249=CARTESIAN_POINT('',(-27.482958713852,23.5538899792342,-52.2791635220347));
#56250=CARTESIAN_POINT('Ctrl Pts',(-27.4893929762737,23.5491656528098,-53.5291635220347));
#56251=CARTESIAN_POINT('Ctrl Pts',(-27.4896080253726,23.4904443261825,-53.5261802051937));
#56252=CARTESIAN_POINT('Ctrl Pts',(-27.4884091334729,23.431731975206,-53.5231968883528));
#56253=CARTESIAN_POINT('Ctrl Pts',(-27.4270986390246,22.0698132025148,-53.4539179343869));
#56254=CARTESIAN_POINT('Ctrl Pts',(-25.8862801146668,19.5273523385874,-53.3213266601369));
#56255=CARTESIAN_POINT('Ctrl Pts',(-21.4284410418566,19.4103652344728,-53.1224397487623));
#56256=CARTESIAN_POINT('Ctrl Pts',(-18.920366828257,23.097583551946,-52.9235528373871));
#56257=CARTESIAN_POINT('Ctrl Pts',(-20.6667650265468,27.2007662818071,-52.7246659260124));
#56258=CARTESIAN_POINT('Ctrl Pts',(-25.0628437626404,27.9494363878393,-52.5257790146374));
#56259=CARTESIAN_POINT('Ctrl Pts',(-27.3074034903904,25.4900842062352,-52.3772782133115));
#56260=CARTESIAN_POINT('Ctrl Pts',(-27.4858519506129,23.8683743917818,-52.2950730491106));
#56261=CARTESIAN_POINT('Ctrl Pts',(-27.482958713852,23.5538899792342,-52.2791635220347));
#56262=CARTESIAN_POINT('',(-27.476795898706,23.5497105560713,-51.0291635220347));
#56263=CARTESIAN_POINT('Ctrl Pts',(-27.482958713852,23.5538899792342,-52.2791635220347));
#56264=CARTESIAN_POINT('Ctrl Pts',(-27.4737957170429,22.557905237283,-52.2287774119857));
#56265=CARTESIAN_POINT('Ctrl Pts',(-26.5831973659458,20.2368697433501,-52.1120956648117));
#56266=CARTESIAN_POINT('Ctrl Pts',(-22.677522633219,18.9808878760329,-51.9291182805128));
#56267=CARTESIAN_POINT('Ctrl Pts',(-19.2342218731823,21.8145595326581,-51.7302313691379));
#56268=CARTESIAN_POINT('Ctrl Pts',(-19.7569873492678,26.2431858929006,-51.5313444577628));
#56269=CARTESIAN_POINT('Ctrl Pts',(-23.7654419121505,28.1972348172902,-51.3324575463881));
#56270=CARTESIAN_POINT('Ctrl Pts',(-26.9727382800942,26.2478552605321,-51.1650639011454));
#56271=CARTESIAN_POINT('Ctrl Pts',(-27.4759497159671,24.2403761058591,-51.0639658930275));
#56272=CARTESIAN_POINT('Ctrl Pts',(-27.476795898706,23.5497105560713,-51.0291635220347));
#56273=CARTESIAN_POINT('',(-27.483338271532,23.546803532641,-49.7791635651174));
#56274=CARTESIAN_POINT('Ctrl Pts',(-27.476795898706,23.5497105560713,-51.0291635220347));
#56275=CARTESIAN_POINT('Ctrl Pts',(-27.4775616240699,22.9247153805349,-50.9976702559025));
#56276=CARTESIAN_POINT('Ctrl Pts',(-27.0416309458266,20.9850685926429,-50.8998813526456));
#56277=CARTESIAN_POINT('Ctrl Pts',(-23.9969628335229,18.9197881124001,-50.7357968122635));
#56278=CARTESIAN_POINT('Ctrl Pts',(-19.8960309801959,20.6714653418028,-50.5369099008885));
#56279=CARTESIAN_POINT('Ctrl Pts',(-19.1530189058048,25.0685039178133,-50.3380229895135));
#56280=CARTESIAN_POINT('Ctrl Pts',(-22.450691709674,28.0703981964692,-50.1391360781388));
#56281=CARTESIAN_POINT('Ctrl Pts',(-26.4858247139179,26.9916313974245,-49.9528498692994));
#56282=CARTESIAN_POINT('Ctrl Pts',(-27.4752038925693,24.6068284845104,-49.8328592975852));
#56283=CARTESIAN_POINT('Ctrl Pts',(-27.4849541685477,23.546817866354,-49.7791643629959));
#56284=CARTESIAN_POINT('',(-27.4850065049564,23.5523966888927,-48.5291629058911));
#56285=CARTESIAN_POINT('Ctrl Pts',(-27.4832510187351,23.5468027586706,-49.7791635220347));
#56286=CARTESIAN_POINT('Ctrl Pts',(-27.4831011760015,23.3759708690314,-49.7705061923292));
#56287=CARTESIAN_POINT('Ctrl Pts',(-27.4718178556067,23.2056082410999,-49.7618488626238));
#56288=CARTESIAN_POINT('Ctrl Pts',(-27.449602469036,23.0368724910297,-49.7531915329183));
#56289=CARTESIAN_POINT('Ctrl Pts',(-27.4394841846031,22.9600196166593,-49.7492484404086));
#56290=CARTESIAN_POINT('Ctrl Pts',(-27.4270986677299,22.8835037321968,-49.7453053478988));
#56291=CARTESIAN_POINT('Ctrl Pts',(-27.4124678417013,22.8074322982954,-49.741362255389));
#56292=CARTESIAN_POINT('Ctrl Pts',(-27.3906787116914,22.6941420192582,-49.7354899584203));
#56293=CARTESIAN_POINT('Ctrl Pts',(-27.3638641407678,22.5816214712891,-49.7296176614516));
#56294=CARTESIAN_POINT('Ctrl Pts',(-27.332090953477,22.4703510771497,-49.7237453644829));
#56295=CARTESIAN_POINT('Ctrl Pts',(-27.3003589417136,22.3592248806043,-49.7178806775447));
#56296=CARTESIAN_POINT('Ctrl Pts',(-27.2636812049932,22.2493460099168,-49.7120159906065));
#56297=CARTESIAN_POINT('Ctrl Pts',(-27.2221757967736,22.1411859841641,-49.7061513036684));
#56298=CARTESIAN_POINT('Ctrl Pts',(-27.1807130742681,22.033137194227,-49.7002926481936));
#56299=CARTESIAN_POINT('Ctrl Pts',(-27.1344327030313,21.9268041167515,-49.6944339927187));
#56300=CARTESIAN_POINT('Ctrl Pts',(-27.0835026988673,21.82264370555,-49.6885753372439));
#56301=CARTESIAN_POINT('Ctrl Pts',(-27.030583323882,21.7144146969434,-49.682487837526));
#56302=CARTESIAN_POINT('Ctrl Pts',(-26.9726437983051,21.6085319845137,-49.6764003378081));
#56303=CARTESIAN_POINT('Ctrl Pts',(-26.9099281291323,21.5054863152335,-49.6703128380902));
#56304=CARTESIAN_POINT('Ctrl Pts',(-26.8496400034323,21.4064292479272,-49.6644609680068));
#56305=CARTESIAN_POINT('Ctrl Pts',(-26.784938835661,21.3099940660363,-49.6586090979234));
#56306=CARTESIAN_POINT('Ctrl Pts',(-26.7160880971187,21.2165914224726,-49.65275722784));
#56307=CARTESIAN_POINT('Ctrl Pts',(-26.6472478417273,21.1232030003107,-49.646906248757));
#56308=CARTESIAN_POINT('Ctrl Pts',(-26.5742595170202,21.0328465310636,-49.6410552696741));
#56309=CARTESIAN_POINT('Ctrl Pts',(-26.4974289986125,20.9459023492412,-49.6352042905911));
#56310=CARTESIAN_POINT('Ctrl Pts',(-26.4205915724017,20.8589503503001,-49.6293527854488));
#56311=CARTESIAN_POINT('Ctrl Pts',(-26.339911539517,20.7754115584539,-49.6235012803065));
#56312=CARTESIAN_POINT('Ctrl Pts',(-26.2557335225697,20.6956314345937,-49.6176497751642));
#56313=CARTESIAN_POINT('Ctrl Pts',(-26.1715275519354,20.6158248174911,-49.6117963268645));
#56314=CARTESIAN_POINT('Ctrl Pts',(-26.0838215873411,20.5397796344981,-49.6059428785647));
#56315=CARTESIAN_POINT('Ctrl Pts',(-25.9929948417721,20.4678023688278,-49.6000894302649));
#56316=CARTESIAN_POINT('Ctrl Pts',(-25.9020648064708,20.3957432493769,-49.5942293253234));
#56317=CARTESIAN_POINT('Ctrl Pts',(-25.8080072306637,20.3277615377149,-49.5883692203818));
#56318=CARTESIAN_POINT('Ctrl Pts',(-25.7112320163825,20.2641215746634,-49.5825091154403));
#56319=CARTESIAN_POINT('Ctrl Pts',(-25.6143916300514,20.2004387540798,-49.5766450640848));
#56320=CARTESIAN_POINT('Ctrl Pts',(-25.5148303152712,20.1411037152761,-49.5707810127294));
#56321=CARTESIAN_POINT('Ctrl Pts',(-25.4129828486518,20.0863349855787,-49.5649169613739));
#56322=CARTESIAN_POINT('Ctrl Pts',(-25.3109852791974,20.0314855377067,-49.5590442675774));
#56323=CARTESIAN_POINT('Ctrl Pts',(-25.206695204351,19.9812160091992,-49.5531715737808));
#56324=CARTESIAN_POINT('Ctrl Pts',(-25.1005677120735,19.9356969792804,-49.5472988799842));
#56325=CARTESIAN_POINT('Ctrl Pts',(-25.0715117799823,19.9232346303283,-49.5456910346608));
#56326=CARTESIAN_POINT('Ctrl Pts',(-25.0423182071403,19.9111280771821,-49.5440831893374));
#56327=CARTESIAN_POINT('Ctrl Pts',(-25.0129965121013,19.8993801636453,-49.542475344014));
#56328=CARTESIAN_POINT('Ctrl Pts',(-24.9059055510578,19.8564735257707,-49.5366030470453));
#56329=CARTESIAN_POINT('Ctrl Pts',(-24.7967457138194,19.8182109479283,-49.5307307500766));
#56330=CARTESIAN_POINT('Ctrl Pts',(-24.685957309616,19.7847958983753,-49.5248584531079));
#56331=CARTESIAN_POINT('Ctrl Pts',(-24.5753124783859,19.7514241520727,-49.5189937661697));
#56332=CARTESIAN_POINT('Ctrl Pts',(-24.4630436693248,19.7228875596612,-49.5131290792315));
#56333=CARTESIAN_POINT('Ctrl Pts',(-24.3496113922415,19.699341676836,-49.5072643922933));
#56334=CARTESIAN_POINT('Ctrl Pts',(-24.2362957731543,19.6758200094774,-49.5014057368185));
#56335=CARTESIAN_POINT('Ctrl Pts',(-24.1218194683739,19.6572789261479,-49.4955470813437));
#56336=CARTESIAN_POINT('Ctrl Pts',(-24.0066577404742,19.6438240752396,-49.4896884258689));
#56337=CARTESIAN_POINT('Ctrl Pts',(-23.8869976940492,19.6298436660039,-49.483600926151));
#56338=CARTESIAN_POINT('Ctrl Pts',(-23.7665980217507,19.6213550662404,-49.477513426433));
#56339=CARTESIAN_POINT('Ctrl Pts',(-23.6460034933658,19.6184182583125,-49.4714259267151));
#56340=CARTESIAN_POINT('Ctrl Pts',(-23.5300768329011,19.6155951257868,-49.4655740566318));
#56341=CARTESIAN_POINT('Ctrl Pts',(-23.4139705723056,19.6179019998154,-49.4597221865484));
#56342=CARTESIAN_POINT('Ctrl Pts',(-23.2981726181708,19.6253391928805,-49.453870316465));
#56343=CARTESIAN_POINT('Ctrl Pts',(-23.1823922953274,19.6327752535653,-49.448019337382));
#56344=CARTESIAN_POINT('Ctrl Pts',(-23.0669205980278,19.6453400536469,-49.4421683582991));
#56345=CARTESIAN_POINT('Ctrl Pts',(-22.9522428468135,19.6629818417642,-49.4363173792161));
#56346=CARTESIAN_POINT('Ctrl Pts',(-22.8375547849657,19.6806252160481,-49.4304658740738));
#56347=CARTESIAN_POINT('Ctrl Pts',(-22.7236612197076,19.7033464229298,-49.4246143689316));
#56348=CARTESIAN_POINT('Ctrl Pts',(-22.611039076214,19.7310422618812,-49.4187628637893));
#56349=CARTESIAN_POINT('Ctrl Pts',(-22.4983795333581,19.7587472980178,-49.4129094154895));
#56350=CARTESIAN_POINT('Ctrl Pts',(-22.3869926530182,19.7914301523915,-49.4070559671897));
#56351=CARTESIAN_POINT('Ctrl Pts',(-22.2773412653584,19.8289374539246,-49.40120251889));
#56352=CARTESIAN_POINT('Ctrl Pts',(-22.1675651802605,19.8664874094041,-49.3953424139485));
#56353=CARTESIAN_POINT('Ctrl Pts',(-22.0595289185181,19.9088726289492,-49.3894823090069));
#56354=CARTESIAN_POINT('Ctrl Pts',(-21.9536764439244,19.9558911425234,-49.3836222040654));
#56355=CARTESIAN_POINT('Ctrl Pts',(-21.8477526843142,20.0029413201238,-49.37775815271));
#56356=CARTESIAN_POINT('Ctrl Pts',(-21.7440160092884,20.0546308208483,-49.3718941013545));
#56357=CARTESIAN_POINT('Ctrl Pts',(-21.6428852847426,20.1107119831243,-49.3660300499991));
#56358=CARTESIAN_POINT('Ctrl Pts',(-21.5416055136963,20.1668757978387,-49.3601573562026));
#56359=CARTESIAN_POINT('Ctrl Pts',(-21.4429397093039,20.2274439763767,-49.354284662406));
#56360=CARTESIAN_POINT('Ctrl Pts',(-21.347277377064,20.2921258509032,-49.3484119686095));
#56361=CARTESIAN_POINT('Ctrl Pts',(-21.3210866307305,20.309834666154,-49.346804123286));
#56362=CARTESIAN_POINT('Ctrl Pts',(-21.2951208207174,20.3278516035943,-49.3451962779626));
#56363=CARTESIAN_POINT('Ctrl Pts',(-21.269387484746,20.3461701923012,-49.3435884326392));
#56364=CARTESIAN_POINT('Ctrl Pts',(-21.1754022060517,20.4130747579131,-49.3377161356705));
#56365=CARTESIAN_POINT('Ctrl Pts',(-21.0842057376923,20.484230215103,-49.3318438387018));
#56366=CARTESIAN_POINT('Ctrl Pts',(-20.9962072667315,20.5593761075467,-49.3259715417331));
#56367=CARTESIAN_POINT('Ctrl Pts',(-20.9083228348004,20.6344246168817,-49.3201068547949));
#56368=CARTESIAN_POINT('Ctrl Pts',(-20.8236284701001,20.7134530116684,-49.3142421678567));
#56369=CARTESIAN_POINT('Ctrl Pts',(-20.7425039693215,20.7961579417257,-49.3083774809185));
#56370=CARTESIAN_POINT('Ctrl Pts',(-20.6614629000135,20.8787778149397,-49.3025188254436));
#56371=CARTESIAN_POINT('Ctrl Pts',(-20.5839846797925,20.9650664093115,-49.2966601699688));
#56372=CARTESIAN_POINT('Ctrl Pts',(-20.5104150919925,21.054680985898,-49.290801514494));
#56373=CARTESIAN_POINT('Ctrl Pts',(-20.4339718112937,21.1477959867776,-49.2847140147761));
#56374=CARTESIAN_POINT('Ctrl Pts',(-20.3617490829071,21.2445018031483,-49.2786265150582));
#56375=CARTESIAN_POINT('Ctrl Pts',(-20.2940918421659,21.3443725340582,-49.2725390153403));
#56376=CARTESIAN_POINT('Ctrl Pts',(-20.2290534189436,21.4403775557422,-49.2666871452569));
#56377=CARTESIAN_POINT('Ctrl Pts',(-20.1682338748234,21.5393066640488,-49.2608352751735));
#56378=CARTESIAN_POINT('Ctrl Pts',(-20.1118972068984,21.640749543886,-49.2549834050901));
#56379=CARTESIAN_POINT('Ctrl Pts',(-20.0555691167434,21.7421769781224,-49.2491324260071));
#56380=CARTESIAN_POINT('Ctrl Pts',(-20.0037227462841,21.8461170615773,-49.2432814469241));
#56381=CARTESIAN_POINT('Ctrl Pts',(-19.9565768925592,21.9521335121317,-49.2374304678412));
#56382=CARTESIAN_POINT('Ctrl Pts',(-19.9094267999683,22.0581594945852,-49.2315789626989));
#56383=CARTESIAN_POINT('Ctrl Pts',(-19.866978232227,22.1662618375114,-49.2257274575566));
#56384=CARTESIAN_POINT('Ctrl Pts',(-19.8294021632746,22.2759835114981,-49.2198759524143));
#56385=CARTESIAN_POINT('Ctrl Pts',(-19.7918136161277,22.3857416216642,-49.2140225041145));
#56386=CARTESIAN_POINT('Ctrl Pts',(-19.7591009190245,22.4971197412845,-49.2081690558147));
#56387=CARTESIAN_POINT('Ctrl Pts',(-19.7313852176287,22.609645580007,-49.202315607515));
#56388=CARTESIAN_POINT('Ctrl Pts',(-19.7036379974621,22.7222993850426,-49.1964555025734));
#56389=CARTESIAN_POINT('Ctrl Pts',(-19.6808992143611,22.836103112707,-49.1905953976319));
#56390=CARTESIAN_POINT('Ctrl Pts',(-19.6632389287966,22.950574075445,-49.1847352926903));
#56391=CARTESIAN_POINT('Ctrl Pts',(-19.6455667501352,23.065122127212,-49.1788712413349));
#56392=CARTESIAN_POINT('Ctrl Pts',(-19.6329799237928,23.1803378988461,-49.1730071899794));
#56393=CARTESIAN_POINT('Ctrl Pts',(-19.6254965027066,23.2957351198625,-49.167143138624));
#56394=CARTESIAN_POINT('Ctrl Pts',(-19.6180020525515,23.4113024133472,-49.1612704448274));
#56395=CARTESIAN_POINT('Ctrl Pts',(-19.6156260273691,23.5270512781892,-49.1553977510308));
#56396=CARTESIAN_POINT('Ctrl Pts',(-19.6183344276671,23.64249689859,-49.1495250572343));
#56397=CARTESIAN_POINT('Ctrl Pts',(-19.6190759423627,23.6741039782867,-49.1479172119109));
#56398=CARTESIAN_POINT('Ctrl Pts',(-19.6201982730429,23.7056883683887,-49.1463093665876));
#56399=CARTESIAN_POINT('Ctrl Pts',(-19.6217000500697,23.7372402294764,-49.1447015212642));
#56400=CARTESIAN_POINT('Ctrl Pts',(-19.6271849562072,23.8524763753493,-49.1388292242955));
#56401=CARTESIAN_POINT('Ctrl Pts',(-19.637753678964,23.9676640354022,-49.1329569273268));
#56402=CARTESIAN_POINT('Ctrl Pts',(-19.653408275019,24.082318166008,-49.1270846303581));
#56403=CARTESIAN_POINT('Ctrl Pts',(-19.6690425839608,24.1968237139662,-49.1212199434199));
#56404=CARTESIAN_POINT('Ctrl Pts',(-19.6897496038834,24.3107967016452,-49.1153552564817));
#56405=CARTESIAN_POINT('Ctrl Pts',(-19.7154794174018,24.4237536260841,-49.1094905695435));
#56406=CARTESIAN_POINT('Ctrl Pts',(-19.7411827694178,24.5365943813974,-49.1036319140686));
#56407=CARTESIAN_POINT('Ctrl Pts',(-19.7718985490698,24.6484207513093,-49.0977732585938));
#56408=CARTESIAN_POINT('Ctrl Pts',(-19.8075253148856,24.7587565575709,-49.091914603119));
#56409=CARTESIAN_POINT('Ctrl Pts',(-19.8445436935537,24.8734021776075,-49.0858271034011));
#56410=CARTESIAN_POINT('Ctrl Pts',(-19.8868644729888,24.9864379641687,-49.0797396036832));
#56411=CARTESIAN_POINT('Ctrl Pts',(-19.9343157877445,25.0973434998517,-49.0736521039653));
#56412=CARTESIAN_POINT('Ctrl Pts',(-19.9799303983572,25.2039562007014,-49.0678002338819));
#56413=CARTESIAN_POINT('Ctrl Pts',(-20.0302855751122,25.3086000805575,-49.0619483637985));
#56414=CARTESIAN_POINT('Ctrl Pts',(-20.0851788146588,25.4108312415343,-49.0560964937151));
#56415=CARTESIAN_POINT('Ctrl Pts',(-20.1400636962105,25.5130468368873,-49.0502455146321));
#56416=CARTESIAN_POINT('Ctrl Pts',(-20.1994850711967,25.6128500796862,-49.0443945355491));
#56417=CARTESIAN_POINT('Ctrl Pts',(-20.2631941572255,25.7098210633308,-49.0385435564661));
#56418=CARTESIAN_POINT('Ctrl Pts',(-20.3269089713142,25.8068007656001,-49.0326920513238));
#56419=CARTESIAN_POINT('Ctrl Pts',(-20.3949120357993,25.9009473569887,-49.0268405461815));
#56420=CARTESIAN_POINT('Ctrl Pts',(-20.4669112628304,25.9918699504807,-49.0209890410392));
#56421=CARTESIAN_POINT('Ctrl Pts',(-20.5389343992375,26.0828227373867,-49.0151355927394));
#56422=CARTESIAN_POINT('Ctrl Pts',(-20.6149560804299,26.1705490736297,-49.0092821444397));
#56423=CARTESIAN_POINT('Ctrl Pts',(-20.6946444449772,26.2546917443733,-49.0034286961399));
#56424=CARTESIAN_POINT('Ctrl Pts',(-20.774423432499,26.3389301036048,-48.9975685911984));
#56425=CARTESIAN_POINT('Ctrl Pts',(-20.8578771417787,26.4195763626296,-48.9917084862568));
#56426=CARTESIAN_POINT('Ctrl Pts',(-20.9446373503323,26.4963106653121,-48.9858483813153));
#56427=CARTESIAN_POINT('Ctrl Pts',(-21.0314559864561,26.5730966437448,-48.9799843299598));
#56428=CARTESIAN_POINT('Ctrl Pts',(-21.1215852350192,26.6459651608429,-48.9741202786043));
#56429=CARTESIAN_POINT('Ctrl Pts',(-21.2146257468817,26.7146381785562,-48.9682562272489));
#56430=CARTESIAN_POINT('Ctrl Pts',(-21.307803381886,26.7834124065892,-48.9623835334523));
#56431=CARTESIAN_POINT('Ctrl Pts',(-21.4039005016028,26.8479785648305,-48.9565108396557));
#56432=CARTESIAN_POINT('Ctrl Pts',(-21.5024908441997,26.9081031941313,-48.9506381458592));
#56433=CARTESIAN_POINT('Ctrl Pts',(-21.5294832307866,26.924564311871,-48.9490303005359));
#56434=CARTESIAN_POINT('Ctrl Pts',(-21.5566623754204,26.9406927780457,-48.9474224552126));
#56435=CARTESIAN_POINT('Ctrl Pts',(-21.5840192596848,26.9564844263313,-48.9458146098894));
#56436=CARTESIAN_POINT('Ctrl Pts',(-21.6839341869571,27.0141599048219,-48.9399423129207));
#56437=CARTESIAN_POINT('Ctrl Pts',(-21.7865563406964,27.067532074452,-48.934070015952));
#56438=CARTESIAN_POINT('Ctrl Pts',(-21.8914787572833,27.1163370182602,-48.9281977189833));
#56439=CARTESIAN_POINT('Ctrl Pts',(-21.9962652027512,27.1650787147373,-48.9223330320451));
#56440=CARTESIAN_POINT('Ctrl Pts',(-22.1033456116534,27.2092647829473,-48.9164683451069));
#56441=CARTESIAN_POINT('Ctrl Pts',(-22.2122862223738,27.2486758653762,-48.9106036581687));
#56442=CARTESIAN_POINT('Ctrl Pts',(-22.3211147944957,27.288046415974,-48.9047450026939));
#56443=CARTESIAN_POINT('Ctrl Pts',(-22.4317993767891,27.3226516087894,-48.8988863472191));
#56444=CARTESIAN_POINT('Ctrl Pts',(-22.5438845190874,27.3523193937051,-48.8930276917442));
#56445=CARTESIAN_POINT('Ctrl Pts',(-22.6603478057673,27.3831460284308,-48.8869401920263));
#56446=CARTESIAN_POINT('Ctrl Pts',(-22.7783228849336,27.4086414811871,-48.8808526923084));
#56447=CARTESIAN_POINT('Ctrl Pts',(-22.8972790201337,27.4286690375894,-48.8747651925905));
#56448=CARTESIAN_POINT('Ctrl Pts',(-23.0116307049094,27.4479213847902,-48.8689133225071));
#56449=CARTESIAN_POINT('Ctrl Pts',(-23.1268884645165,27.4621211829458,-48.8630614524237));
#56450=CARTESIAN_POINT('Ctrl Pts',(-23.2425693785703,27.4711988558975,-48.8572095823403));
#56451=CARTESIAN_POINT('Ctrl Pts',(-23.358232679153,27.480275146691,-48.8513586032574));
#56452=CARTESIAN_POINT('Ctrl Pts',(-23.474318594074,27.4842308306213,-48.8455076241744));
#56453=CARTESIAN_POINT('Ctrl Pts',(-23.5903393714356,27.4830482351702,-48.8396566450915));
#56454=CARTESIAN_POINT('Ctrl Pts',(-23.7063705801816,27.4818655333925,-48.8338051399492));
#56455=CARTESIAN_POINT('Ctrl Pts',(-23.8223362263402,27.4755436380719,-48.8279536348069));
#56456=CARTESIAN_POINT('Ctrl Pts',(-23.9377495642408,27.4641169966147,-48.8221021296646));
#56457=CARTESIAN_POINT('Ctrl Pts',(-24.0532012283986,27.4526865606186,-48.8162486813648));
#56458=CARTESIAN_POINT('Ctrl Pts',(-24.1680998084462,27.4361480484437,-48.810395233065));
#56459=CARTESIAN_POINT('Ctrl Pts',(-24.2819653883767,27.4145875709171,-48.8045417847653));
#56460=CARTESIAN_POINT('Ctrl Pts',(-24.3959604581968,27.3930025744457,-48.7986816798237));
#56461=CARTESIAN_POINT('Ctrl Pts',(-24.5089197767366,27.3663842904624,-48.7928215748822));
#56462=CARTESIAN_POINT('Ctrl Pts',(-24.6203752037998,27.3348696149201,-48.7869614699407));
#56463=CARTESIAN_POINT('Ctrl Pts',(-24.7319056891174,27.3033337162163,-48.7810974185852));
#56464=CARTESIAN_POINT('Ctrl Pts',(-24.8419298748564,27.2668949897968,-48.7752333672298));
#56465=CARTESIAN_POINT('Ctrl Pts',(-24.9499979778003,27.2257391234403,-48.7693693158743));
#56466=CARTESIAN_POINT('Ctrl Pts',(-25.0582253515555,27.1845226015523,-48.7634966220778));
#56467=CARTESIAN_POINT('Ctrl Pts',(-25.1644905108437,27.1385752280766,-48.7576239282812));
#56468=CARTESIAN_POINT('Ctrl Pts',(-25.2683666299751,27.0881294296781,-48.7517512344847));
#56469=CARTESIAN_POINT('Ctrl Pts',(-25.2968061737587,27.0743182139314,-48.7501433891613));
#56470=CARTESIAN_POINT('Ctrl Pts',(-25.3250668028408,27.0601700632334,-48.7485355438379));
#56471=CARTESIAN_POINT('Ctrl Pts',(-25.353140137187,27.0456903128542,-48.7469276985145));
#56472=CARTESIAN_POINT('Ctrl Pts',(-25.4556717388197,26.9928062493039,-48.7410554015458));
#56473=CARTESIAN_POINT('Ctrl Pts',(-25.5560462651788,26.9353184298351,-48.7351831045771));
#56474=CARTESIAN_POINT('Ctrl Pts',(-25.6538216974083,26.873426581463,-48.7293108076084));
#56475=CARTESIAN_POINT('Ctrl Pts',(-25.7514704204429,26.811614940011,-48.7234461206702));
#56476=CARTESIAN_POINT('Ctrl Pts',(-25.8465264014651,26.745410838428,-48.717581433732));
#56477=CARTESIAN_POINT('Ctrl Pts',(-25.9385706247761,26.6750606356036,-48.7117167467938));
#56478=CARTESIAN_POINT('Ctrl Pts',(-26.0305201863655,26.6047827835588,-48.705858091319));
#56479=CARTESIAN_POINT('Ctrl Pts',(-26.1194638246777,26.530367561117,-48.6999994358442));
#56480=CARTESIAN_POINT('Ctrl Pts',(-26.2050106009395,26.4521051457628,-48.6941407803694));
#56481=CARTESIAN_POINT('Ctrl Pts',(-26.2938989096307,26.3707857315322,-48.6880532806515));
#56482=CARTESIAN_POINT('Ctrl Pts',(-26.3791191934116,26.2853126910584,-48.6819657809336));
#56483=CARTESIAN_POINT('Ctrl Pts',(-26.4602695466242,26.1960586419029,-48.6758782812157));
#56484=CARTESIAN_POINT('Ctrl Pts',(-26.5382788026781,26.1102593607073,-48.6700264111323));
#56485=CARTESIAN_POINT('Ctrl Pts',(-26.6125270363051,26.0209666666019,-48.6641745410489));
#56486=CARTESIAN_POINT('Ctrl Pts',(-26.6826946729749,25.9285492397458,-48.6583226709655));
#56487=CARTESIAN_POINT('Ctrl Pts',(-26.7528516259839,25.8361458842832,-48.6524716918825));
#56488=CARTESIAN_POINT('Ctrl Pts',(-26.8189289674899,25.7406190711998,-48.6466207127995));
#56489=CARTESIAN_POINT('Ctrl Pts',(-26.8806481787288,25.6423696016052,-48.6407697337166));
#56490=CARTESIAN_POINT('Ctrl Pts',(-26.9423729391188,25.5441112984377,-48.6349182285743));
#56491=CARTESIAN_POINT('Ctrl Pts',(-26.9997385703967,25.4431302021994,-48.629066723432));
#56492=CARTESIAN_POINT('Ctrl Pts',(-27.0525109470736,25.3398544404728,-48.6232152182897));
#56493=CARTESIAN_POINT('Ctrl Pts',(-27.1053008483081,25.2365443831139,-48.6173617699899));
#56494=CARTESIAN_POINT('Ctrl Pts',(-27.1534942739404,25.1309385129752,-48.6115083216901));
#56495=CARTESIAN_POINT('Ctrl Pts',(-27.1969042555072,25.0234871379983,-48.6056548733904));
#56496=CARTESIAN_POINT('Ctrl Pts',(-27.2403636036492,24.9159135674754,-48.5997947684488));
#56497=CARTESIAN_POINT('Ctrl Pts',(-27.2790284950821,24.8064906866064,-48.5939346635073));
#56498=CARTESIAN_POINT('Ctrl Pts',(-27.3127610530459,24.695686347659,-48.5880745585658));
#56499=CARTESIAN_POINT('Ctrl Pts',(-27.3465163277763,24.5848073889242,-48.5822105072103));
#56500=CARTESIAN_POINT('Ctrl Pts',(-27.3753325525098,24.4725455190721,-48.5763464558549));
#56501=CARTESIAN_POINT('Ctrl Pts',(-27.3991228225941,24.3593795203853,-48.5704824044994));
#56502=CARTESIAN_POINT('Ctrl Pts',(-27.4229481547874,24.2460467376067,-48.5646097107029));
#56503=CARTESIAN_POINT('Ctrl Pts',(-27.4417326820611,24.1318075729435,-48.5587370169063));
#56504=CARTESIAN_POINT('Ctrl Pts',(-27.4554412314881,24.0171467584755,-48.5528643231097));
#56505=CARTESIAN_POINT('Ctrl Pts',(-27.4591944030053,23.9857545455146,-48.5512564777864));
#56506=CARTESIAN_POINT('Ctrl Pts',(-27.4625673945139,23.9543307288691,-48.549648632463));
#56507=CARTESIAN_POINT('Ctrl Pts',(-27.4655601649022,23.9228852427422,-48.5480407871396));
#56508=CARTESIAN_POINT('Ctrl Pts',(-27.4772725933714,23.7998210048773,-48.541748365438));
#56509=CARTESIAN_POINT('Ctrl Pts',(-27.4831841036996,23.6761959820669,-48.5354559437363));
#56510=CARTESIAN_POINT('Ctrl Pts',(-27.4832519411198,23.5524078640301,-48.5291635220346));
#56511=CARTESIAN_POINT('',(-27.4815091528986,23.5526679104256,-47.2791640449873));
#56512=CARTESIAN_POINT('Ctrl Pts',(-27.4882898507423,23.5523757766641,-48.5291617528909));
#56513=CARTESIAN_POINT('Ctrl Pts',(-27.4804866516216,22.3704529683091,-48.4691591271821));
#56514=CARTESIAN_POINT('Ctrl Pts',(-26.2851771232687,19.8689985368499,-48.3428608643485));
#56515=CARTESIAN_POINT('Ctrl Pts',(-22.0263435048847,19.154976418624,-48.1502669643898));
#56516=CARTESIAN_POINT('Ctrl Pts',(-19.0286955606611,22.456509696377,-47.9513800530149));
#56517=CARTESIAN_POINT('Ctrl Pts',(-20.1859751080046,26.7630999056849,-47.75249314164));
#56518=CARTESIAN_POINT('Ctrl Pts',(-24.4347403640322,28.117355782832,-47.5536062302651));
#56519=CARTESIAN_POINT('Ctrl Pts',(-27.1604995493759,25.8623944274898,-47.3958301919578));
#56520=CARTESIAN_POINT('Ctrl Pts',(-27.4810072727968,24.0520277401451,-47.3043497907753));
#56521=CARTESIAN_POINT('Ctrl Pts',(-27.4782377188801,23.5526853739332,-47.2791650267177));
#56522=CARTESIAN_POINT('',(-27.4821351592969,23.5471947449596,-46.0291630887908));
#56523=CARTESIAN_POINT('Ctrl Pts',(-27.4832517957162,23.5526586078825,-47.2791635220346));
#56524=CARTESIAN_POINT('Ctrl Pts',(-27.4833234694447,23.4354999231549,-47.273262034116));
#56525=CARTESIAN_POINT('Ctrl Pts',(-27.478155809776,23.3183245754339,-47.2673605461975));
#56526=CARTESIAN_POINT('Ctrl Pts',(-27.4677709458428,23.2016288451683,-47.2614590582789));
#56527=CARTESIAN_POINT('Ctrl Pts',(-27.4573847051595,23.0849176442282,-47.2555567879838));
#56528=CARTESIAN_POINT('Ctrl Pts',(-27.4417799191657,22.9686865891467,-47.2496545176888));
#56529=CARTESIAN_POINT('Ctrl Pts',(-27.4210306059043,22.8534268000984,-47.2437522473937));
#56530=CARTESIAN_POINT('Ctrl Pts',(-27.4002738442678,22.7381256362763,-47.2378478583623));
#56531=CARTESIAN_POINT('Ctrl Pts',(-27.3743689516746,22.6237968291915,-47.2319434693309));
#56532=CARTESIAN_POINT('Ctrl Pts',(-27.3434409454458,22.5109206993227,-47.2260390802996));
#56533=CARTESIAN_POINT('Ctrl Pts',(-27.3124724484287,22.3978967925995,-47.2201269612722));
#56534=CARTESIAN_POINT('Ctrl Pts',(-27.2764678083027,22.286329751818,-47.2142148422447));
#56535=CARTESIAN_POINT('Ctrl Pts',(-27.2356019212984,22.1766845950621,-47.2083027232173));
#56536=CARTESIAN_POINT('Ctrl Pts',(-27.1947089385844,22.066966739203,-47.2023866842196));
#56537=CARTESIAN_POINT('Ctrl Pts',(-27.1489484441694,21.9591736775379,-47.196470645222));
#56538=CARTESIAN_POINT('Ctrl Pts',(-27.0985427249335,21.8537485663107,-47.1905546062243));
#56539=CARTESIAN_POINT('Ctrl Pts',(-27.0480436648253,21.7481282297798,-47.1846276119571));
#56540=CARTESIAN_POINT('Ctrl Pts',(-26.9928823794142,21.6448849629928,-47.1787006176899));
#56541=CARTESIAN_POINT('Ctrl Pts',(-26.9333265762987,21.5444362368349,-47.1727736234227));
#56542=CARTESIAN_POINT('Ctrl Pts',(-26.876583496888,21.4487315406185,-47.1671265514536));
#56543=CARTESIAN_POINT('Ctrl Pts',(-26.8158517014826,21.3555636795958,-47.1614794794845));
#56544=CARTESIAN_POINT('Ctrl Pts',(-26.751396921784,21.2652659685397,-47.1558324075154));
#56545=CARTESIAN_POINT('Ctrl Pts',(-26.6843714598259,21.1713668686499,-47.1499601105467));
#56546=CARTESIAN_POINT('Ctrl Pts',(-26.6130986987919,21.0802620473527,-47.144087813578));
#56547=CARTESIAN_POINT('Ctrl Pts',(-26.5378396213827,20.9923603561859,-47.1382155166093));
#56548=CARTESIAN_POINT('Ctrl Pts',(-26.4626780737607,20.9045725786297,-47.1323508296712));
#56549=CARTESIAN_POINT('Ctrl Pts',(-26.3835407493514,20.8199799874659,-47.126486142733));
#56550=CARTESIAN_POINT('Ctrl Pts',(-26.3007314868534,20.7389619886826,-47.1206214557948));
#56551=CARTESIAN_POINT('Ctrl Pts',(-26.2180073884982,20.6580273118395,-47.11476280032));
#56552=CARTESIAN_POINT('Ctrl Pts',(-26.1316191571331,20.5806602024921,-47.1089041448452));
#56553=CARTESIAN_POINT('Ctrl Pts',(-26.0419099764137,20.5072060026096,-47.1030454893704));
#56554=CARTESIAN_POINT('Ctrl Pts',(-25.94869667608,20.4308826169815,-47.0969579896525));
#56555=CARTESIAN_POINT('Ctrl Pts',(-25.8518979947514,20.3587844012713,-47.0908704899346));
#56556=CARTESIAN_POINT('Ctrl Pts',(-25.7519402769323,20.2912557424248,-47.0847829902167));
#56557=CARTESIAN_POINT('Ctrl Pts',(-25.6558516353529,20.2263409240615,-47.0789311201333));
#56558=CARTESIAN_POINT('Ctrl Pts',(-25.556844338942,20.165648744379,-47.0730792500499));
#56559=CARTESIAN_POINT('Ctrl Pts',(-25.4553290421953,20.1094426722081,-47.0672273799665));
#56560=CARTESIAN_POINT('Ctrl Pts',(-25.3538292020755,20.0532451579226,-47.0613764008836));
#56561=CARTESIAN_POINT('Ctrl Pts',(-25.2498224824428,20.001532593206,-47.0555254218006));
#56562=CARTESIAN_POINT('Ctrl Pts',(-25.1437454466297,19.9545232134543,-47.0496744427177));
#56563=CARTESIAN_POINT('Ctrl Pts',(-25.0376588734705,19.907509607107,-47.0438229375754));
#56564=CARTESIAN_POINT('Ctrl Pts',(-24.9295019920551,19.8652001938305,-47.0379714324331));
#56565=CARTESIAN_POINT('Ctrl Pts',(-24.8197320514474,19.8277653592613,-47.0321199272909));
#56566=CARTESIAN_POINT('Ctrl Pts',(-24.7099256586321,19.7903180933985,-47.0262664789911));
#56567=CARTESIAN_POINT('Ctrl Pts',(-24.5985055325443,19.7577487583681,-47.0204130306914));
#56568=CARTESIAN_POINT('Ctrl Pts',(-24.4859441190497,19.7301778919323,-47.0145595823916));
#56569=CARTESIAN_POINT('Ctrl Pts',(-24.3732546987856,19.7025756714344,-47.0086994774501));
#56570=CARTESIAN_POINT('Ctrl Pts',(-24.2594218023143,19.6799833637158,-47.0028393725086));
#56571=CARTESIAN_POINT('Ctrl Pts',(-24.1449282069534,19.6624704080079,-46.9969792675671));
#56572=CARTESIAN_POINT('Ctrl Pts',(-24.030357507322,19.6449456584204,-46.9911152162117));
#56573=CARTESIAN_POINT('Ctrl Pts',(-23.9151256328295,19.6325071162445,-46.9852511648562));
#56574=CARTESIAN_POINT('Ctrl Pts',(-23.799718876791,19.6251722086098,-46.9793871135008));
#56575=CARTESIAN_POINT('Ctrl Pts',(-23.6841420342313,19.6178264907855,-46.9735144197042));
#56576=CARTESIAN_POINT('Ctrl Pts',(-23.5683902074797,19.6155994273635,-46.9676417259077));
#56577=CARTESIAN_POINT('Ctrl Pts',(-23.4529481681787,19.6184563949596,-46.9617690321111));
#56578=CARTESIAN_POINT('Ctrl Pts',(-23.4213420689235,19.6192385848963,-46.9601611867876));
#56579=CARTESIAN_POINT('Ctrl Pts',(-23.3897591493249,19.6204015613025,-46.9585533414641));
#56580=CARTESIAN_POINT('Ctrl Pts',(-23.3582092470315,19.621943941879,-46.9569454961405));
#56581=CARTESIAN_POINT('Ctrl Pts',(-23.242980255232,19.6275771434383,-46.9510731991718));
#56582=CARTESIAN_POINT('Ctrl Pts',(-23.1278062916893,19.6382940950095,-46.9452009022031));
#56583=CARTESIAN_POINT('Ctrl Pts',(-23.0131724022755,19.6540962290565,-46.9393286052344));
#56584=CARTESIAN_POINT('Ctrl Pts',(-22.898687069278,19.6698778847927,-46.9334639182962));
#56585=CARTESIAN_POINT('Ctrl Pts',(-22.7847408243035,19.6907315619455,-46.927599231358));
#56586=CARTESIAN_POINT('Ctrl Pts',(-22.6718171056727,19.7166067209404,-46.9217345444197));
#56587=CARTESIAN_POINT('Ctrl Pts',(-22.5590095220178,19.742455268954,-46.9158758889449));
#56588=CARTESIAN_POINT('Ctrl Pts',(-22.4472227735291,19.7733149350178,-46.9100172334701));
#56589=CARTESIAN_POINT('Ctrl Pts',(-22.3369329075138,19.809083664939,-46.9041585779953));
#56590=CARTESIAN_POINT('Ctrl Pts',(-22.2223350221898,19.8462495529556,-46.8980710782774));
#56591=CARTESIAN_POINT('Ctrl Pts',(-22.1093537927857,19.8887157656178,-46.8919835785595));
#56592=CARTESIAN_POINT('Ctrl Pts',(-21.998509415096,19.9363097678848,-46.8858960788416));
#56593=CARTESIAN_POINT('Ctrl Pts',(-21.8919555049896,19.9820615429849,-46.8800442087582));
#56594=CARTESIAN_POINT('Ctrl Pts',(-21.7873765149867,20.032551346582,-46.8741923386748));
#56595=CARTESIAN_POINT('Ctrl Pts',(-21.6852160819991,20.0875761042311,-46.8683404685914));
#56596=CARTESIAN_POINT('Ctrl Pts',(-21.5830712038666,20.1425924838604,-46.8624894895084));
#56597=CARTESIAN_POINT('Ctrl Pts',(-21.483344514405,20.2021422486573,-46.8566385104255));
#56598=CARTESIAN_POINT('Ctrl Pts',(-21.3864555997031,20.2659760760489,-46.8507875313425));
#56599=CARTESIAN_POINT('Ctrl Pts',(-21.2895579737555,20.3298156427158,-46.8449360262002));
#56600=CARTESIAN_POINT('Ctrl Pts',(-21.1954989749873,20.3979398102345,-46.8390845210579));
#56601=CARTESIAN_POINT('Ctrl Pts',(-21.1046691141967,20.4700559879553,-46.8332330159157));
#56602=CARTESIAN_POINT('Ctrl Pts',(-21.0138090907866,20.5421961138888,-46.8273795676159));
#56603=CARTESIAN_POINT('Ctrl Pts',(-20.926180661184,20.6183306291052,-46.8215261193161));
#56604=CARTESIAN_POINT('Ctrl Pts',(-20.8421406128498,20.6981272127412,-46.8156726710164));
#56605=CARTESIAN_POINT('Ctrl Pts',(-20.7580049927315,20.7780145424204,-46.8098125660748));
#56606=CARTESIAN_POINT('Ctrl Pts',(-20.6774661989265,20.8615719680608,-46.8039524611333));
#56607=CARTESIAN_POINT('Ctrl Pts',(-20.6008436134321,20.9484308558532,-46.7980923561918));
#56608=CARTESIAN_POINT('Ctrl Pts',(-20.524169427422,21.0353482376702,-46.7922283048363));
#56609=CARTESIAN_POINT('Ctrl Pts',(-20.4514169600033,21.1255711877167,-46.7863642534809));
#56610=CARTESIAN_POINT('Ctrl Pts',(-20.3828637350648,21.2186999993701,-46.7805002021254));
#56611=CARTESIAN_POINT('Ctrl Pts',(-20.3142094763573,21.3119660643017,-46.7746275083289));
#56612=CARTESIAN_POINT('Ctrl Pts',(-20.2497670411067,21.4081461960695,-46.7687548145323));
#56613=CARTESIAN_POINT('Ctrl Pts',(-20.1897693397026,21.5068138327502,-46.7628821207357));
#56614=CARTESIAN_POINT('Ctrl Pts',(-20.1733429726966,21.5338273811663,-46.7612742754123));
#56615=CARTESIAN_POINT('Ctrl Pts',(-20.1572494973232,21.561027259378,-46.7596664300889));
#56616=CARTESIAN_POINT('Ctrl Pts',(-20.1414930682971,21.5884044436148,-46.7580585847655));
#56617=CARTESIAN_POINT('Ctrl Pts',(-20.0839462203127,21.6883935120077,-46.7521862877968));
#56618=CARTESIAN_POINT('Ctrl Pts',(-20.0307061616155,21.7910842666017,-46.7463139908281));
#56619=CARTESIAN_POINT('Ctrl Pts',(-19.9820362852176,21.8960694044739,-46.7404416938594));
#56620=CARTESIAN_POINT('Ctrl Pts',(-19.9334294811142,22.0009184899451,-46.7345770069212));
#56621=CARTESIAN_POINT('Ctrl Pts',(-19.8893812536582,22.1080556742114,-46.728712319983));
#56622=CARTESIAN_POINT('Ctrl Pts',(-19.8501104019643,22.21704691372,-46.7228476330448));
#56623=CARTESIAN_POINT('Ctrl Pts',(-19.8108799378831,22.3259260625615,-46.71698897757));
#56624=CARTESIAN_POINT('Ctrl Pts',(-19.7764172161789,22.4366550873923,-46.7111303220952));
#56625=CARTESIAN_POINT('Ctrl Pts',(-19.7468937006977,22.5487783170081,-46.7052716666204));
#56626=CARTESIAN_POINT('Ctrl Pts',(-19.7162169706978,22.6652811787297,-46.6991841669025));
#56627=CARTESIAN_POINT('Ctrl Pts',(-19.690873363812,22.7832889708687,-46.6930966671845));
#56628=CARTESIAN_POINT('Ctrl Pts',(-19.6709989112952,22.9022707814716,-46.6870091674666));
#56629=CARTESIAN_POINT('Ctrl Pts',(-19.6518937417681,23.0166471478292,-46.6811572973832));
#56630=CARTESIAN_POINT('Ctrl Pts',(-19.6378422831501,23.13192308603,-46.6753054272999));
#56631=CARTESIAN_POINT('Ctrl Pts',(-19.6289134900614,23.24761558655,-46.6694535572164));
#56632=CARTESIAN_POINT('Ctrl Pts',(-19.6199860564626,23.3632904718349,-46.6636025781335));
#56633=CARTESIAN_POINT('Ctrl Pts',(-19.6161797693585,23.479381381285,-46.6577515990505));
#56634=CARTESIAN_POINT('Ctrl Pts',(-19.6175116735539,23.5954005406634,-46.6519006199675));
#56635=CARTESIAN_POINT('Ctrl Pts',(-19.6188436975003,23.7114301312808,-46.6460491148252));
#56636=CARTESIAN_POINT('Ctrl Pts',(-19.6253148263598,23.8273875456222,-46.6401976096829));
#56637=CARTESIAN_POINT('Ctrl Pts',(-19.6368899863511,23.9427860827516,-46.6343461045406));
#56638=CARTESIAN_POINT('Ctrl Pts',(-19.648468990201,24.058222941223,-46.6284926562408));
#56639=CARTESIAN_POINT('Ctrl Pts',(-19.6651553542235,24.1731001423452,-46.622639207941));
#56640=CARTESIAN_POINT('Ctrl Pts',(-19.6868623500484,24.2869378813265,-46.6167857596412));
#56641=CARTESIAN_POINT('Ctrl Pts',(-19.7085940314411,24.4009050785363,-46.6109256546997));
#56642=CARTESIAN_POINT('Ctrl Pts',(-19.7353576632463,24.5138300478736,-46.6050655497582));
#56643=CARTESIAN_POINT('Ctrl Pts',(-19.7670157471645,24.6252448257043,-46.5992054448166));
#56644=CARTESIAN_POINT('Ctrl Pts',(-19.7986951508208,24.7367346344149,-46.5933413934611));
#56645=CARTESIAN_POINT('Ctrl Pts',(-19.8352754396424,24.8467118352359,-46.5874773421057));
#56646=CARTESIAN_POINT('Ctrl Pts',(-19.8765703471683,24.9547268842891,-46.5816132907502));
#56647=CARTESIAN_POINT('Ctrl Pts',(-19.9179261151446,25.0629011259627,-46.5757405969536));
#56648=CARTESIAN_POINT('Ctrl Pts',(-19.9640102055735,25.1691070665559,-46.569867903157));
#56649=CARTESIAN_POINT('Ctrl Pts',(-20.0145896426912,25.2729181798473,-46.5639952093605));
#56650=CARTESIAN_POINT('Ctrl Pts',(-20.0284374464825,25.301339926117,-46.5623873640372));
#56651=CARTESIAN_POINT('Ctrl Pts',(-20.0426219546968,25.3295823242243,-46.560779518714));
#56652=CARTESIAN_POINT('Ctrl Pts',(-20.0571378212839,25.3576370010077,-46.5591716733908));
#56653=CARTESIAN_POINT('Ctrl Pts',(-20.1101537912445,25.4601004600558,-46.5532993764221));
#56654=CARTESIAN_POINT('Ctrl Pts',(-20.167770737323,25.5604009209406,-46.5474270794533));
#56655=CARTESIAN_POINT('Ctrl Pts',(-20.2297883638258,25.6580966222051,-46.5415547824846));
#56656=CARTESIAN_POINT('Ctrl Pts',(-20.2917256204098,25.7556657175995,-46.5356900955464));
#56657=CARTESIAN_POINT('Ctrl Pts',(-20.3580519968302,25.8506364203737,-46.5298254086083));
#56658=CARTESIAN_POINT('Ctrl Pts',(-20.4285205951604,25.9425900322207,-46.5239607216701));
#56659=CARTESIAN_POINT('Ctrl Pts',(-20.4989167209491,26.0344490755347,-46.5181020661952));
#56660=CARTESIAN_POINT('Ctrl Pts',(-20.5734463453189,26.1232968735865,-46.5122434107204));
#56661=CARTESIAN_POINT('Ctrl Pts',(-20.651818787918,26.2087428613625,-46.5063847552455));
#56662=CARTESIAN_POINT('Ctrl Pts',(-20.7332525271543,26.2975264446805,-46.5002972555276));
#56663=CARTESIAN_POINT('Ctrl Pts',(-20.8188351687312,26.3826366607314,-46.4942097558097));
#56664=CARTESIAN_POINT('Ctrl Pts',(-20.9081935781745,26.46367208372,-46.4881222560918));
#56665=CARTESIAN_POINT('Ctrl Pts',(-20.9940931801707,26.5415708581688,-46.4822703860084));
#56666=CARTESIAN_POINT('Ctrl Pts',(-21.0834813520403,26.6157041175541,-46.476418515925));
#56667=CARTESIAN_POINT('Ctrl Pts',(-21.1759890026619,26.6857527620732,-46.4705666458416));
#56668=CARTESIAN_POINT('Ctrl Pts',(-21.2684825681527,26.7557907410494,-46.4647156667587));
#56669=CARTESIAN_POINT('Ctrl Pts',(-21.364094338535,26.8217450922534,-46.4588646876757));
#56670=CARTESIAN_POINT('Ctrl Pts',(-21.4624231545989,26.8833378129521,-46.4530137085927));
#56671=CARTESIAN_POINT('Ctrl Pts',(-21.5607608113695,26.9449360714289,-46.4471622034505));
#56672=CARTESIAN_POINT('Ctrl Pts',(-21.6618156490959,27.0021717003803,-46.4413106983082));
#56673=CARTESIAN_POINT('Ctrl Pts',(-21.7651592392486,27.0548111254783,-46.4354591931659));
#56674=CARTESIAN_POINT('Ctrl Pts',(-21.8685371475583,27.1074680309836,-46.4296057448661));
#56675=CARTESIAN_POINT('Ctrl Pts',(-21.9742049514397,27.1555255101603,-46.4237522965663));
#56676=CARTESIAN_POINT('Ctrl Pts',(-22.0817121027105,27.1987971742113,-46.4178988482666));
#56677=CARTESIAN_POINT('Ctrl Pts',(-22.1893415129568,27.2421180475405,-46.412038743325));
#56678=CARTESIAN_POINT('Ctrl Pts',(-22.2988140619247,27.2806420882121,-46.4061786383835));
#56679=CARTESIAN_POINT('Ctrl Pts',(-22.4096617202973,27.3142320216698,-46.4003185334419));
#56680=CARTESIAN_POINT('Ctrl Pts',(-22.5205840276297,27.3478445758453,-46.3944544820865));
#56681=CARTESIAN_POINT('Ctrl Pts',(-22.6328828887608,27.3765163044147,-46.3885904307311));
#56682=CARTESIAN_POINT('Ctrl Pts',(-22.7460794099647,27.4001609189533,-46.3827263793757));
#56683=CARTESIAN_POINT('Ctrl Pts',(-22.8594427602453,27.4238403809339,-46.3768536855791));
#56684=CARTESIAN_POINT('Ctrl Pts',(-22.9737060045358,27.442477875726,-46.3709809917825));
#56685=CARTESIAN_POINT('Ctrl Pts',(-23.0883843658929,27.4560388542443,-46.3651082979859));
#56686=CARTESIAN_POINT('Ctrl Pts',(-23.1197813828984,27.4597516233152,-46.3635004526626));
#56687=CARTESIAN_POINT('Ctrl Pts',(-23.1512095143003,27.4630841720209,-46.3618926073392));
#56688=CARTESIAN_POINT('Ctrl Pts',(-23.1826588258506,27.4660364720341,-46.3602847620158));
#56689=CARTESIAN_POINT('Ctrl Pts',(-23.2975204323751,27.4768190903412,-46.3544124650471));
#56690=CARTESIAN_POINT('Ctrl Pts',(-23.4130492948945,27.4825616380405,-46.3485401680784));
#56691=CARTESIAN_POINT('Ctrl Pts',(-23.5287654837693,27.4831938364649,-46.3426678711097));
#56692=CARTESIAN_POINT('Ctrl Pts',(-23.6443317136537,27.4838252156103,-46.3368031841715));
#56693=CARTESIAN_POINT('Ctrl Pts',(-23.7600843775699,27.4793594132309,-46.3309384972333));
#56694=CARTESIAN_POINT('Ctrl Pts',(-23.8755377588109,27.4697778245096,-46.3250738102951));
#56695=CARTESIAN_POINT('Ctrl Pts',(-23.9908724034759,27.4602060898526,-46.3192151548203));
#56696=CARTESIAN_POINT('Ctrl Pts',(-24.1059079681931,27.4455290677664,-46.3133564993455));
#56697=CARTESIAN_POINT('Ctrl Pts',(-24.2201587390104,27.4257801955613,-46.3074978438707));
#56698=CARTESIAN_POINT('Ctrl Pts',(-24.3388722455673,27.4052599150131,-46.3014103441528));
#56699=CARTESIAN_POINT('Ctrl Pts',(-24.4567379442093,27.3792634825815,-46.2953228444349));
#56700=CARTESIAN_POINT('Ctrl Pts',(-24.5732164136781,27.3478878349002,-46.289235344717));
#56701=CARTESIAN_POINT('Ctrl Pts',(-24.6851863360486,27.317726648449,-46.2833834746336));
#56702=CARTESIAN_POINT('Ctrl Pts',(-24.795873987325,27.282595049108,-46.2775316045502));
#56703=CARTESIAN_POINT('Ctrl Pts',(-24.9048113940913,27.2426310724591,-46.2716797344668));
#56704=CARTESIAN_POINT('Ctrl Pts',(-25.0137322141468,27.2026731806891,-46.2658287553838));
#56705=CARTESIAN_POINT('Ctrl Pts',(-25.1209029315755,27.1578845168978,-46.2599777763009));
#56706=CARTESIAN_POINT('Ctrl Pts',(-25.225872814454,27.1084523107965,-46.2541267972179));
#56707=CARTESIAN_POINT('Ctrl Pts',(-25.3308521351355,27.0590156602641,-46.2482752920756));
#56708=CARTESIAN_POINT('Ctrl Pts',(-25.4336298538959,27.0049348136004,-46.2424237869333));
#56709=CARTESIAN_POINT('Ctrl Pts',(-25.5337778769518,26.9464439580895,-46.236572281791));
#56710=CARTESIAN_POINT('Ctrl Pts',(-25.6339591569866,26.8879336790384,-46.2307188334912));
#56711=CARTESIAN_POINT('Ctrl Pts',(-25.7315086481128,26.8250106875082,-46.2248653851914));
#56712=CARTESIAN_POINT('Ctrl Pts',(-25.8260259979156,26.7579532861977,-46.2190119368915));
#56713=CARTESIAN_POINT('Ctrl Pts',(-25.9206508344686,26.6908196260611,-46.21315183195));
#56714=CARTESIAN_POINT('Ctrl Pts',(-26.0122363098395,26.6195424109897,-46.2072917270084));
#56715=CARTESIAN_POINT('Ctrl Pts',(-26.1004139429539,26.5444411991836,-46.2014316220669));
#56716=CARTESIAN_POINT('Ctrl Pts',(-26.1886509581849,26.4692894114122,-46.1955675707115));
#56717=CARTESIAN_POINT('Ctrl Pts',(-26.2734752596195,26.3903087801372,-46.1897035193561));
#56718=CARTESIAN_POINT('Ctrl Pts',(-26.3545553889977,26.3078555641336,-46.1838394680006));
#56719=CARTESIAN_POINT('Ctrl Pts',(-26.4357550143019,26.2252808285485,-46.1779667742041));
#56720=CARTESIAN_POINT('Ctrl Pts',(-26.5131991788765,26.1392236000248,-46.1720940804075));
#56721=CARTESIAN_POINT('Ctrl Pts',(-26.5865967735075,26.0500730542932,-46.166221386611));
#56722=CARTESIAN_POINT('Ctrl Pts',(-26.6066918071259,26.0256651261781,-46.1646135412876));
#56723=CARTESIAN_POINT('Ctrl Pts',(-26.6264837736218,26.0010254957733,-46.1630056959643));
#56724=CARTESIAN_POINT('Ctrl Pts',(-26.645967279281,25.9761625056161,-46.1613978506409));
#56725=CARTESIAN_POINT('Ctrl Pts',(-26.7171035301144,25.8853852124929,-46.1555274446563));
#56726=CARTESIAN_POINT('Ctrl Pts',(-26.7843670858414,25.7913186538014,-46.1496570386717));
#56727=CARTESIAN_POINT('Ctrl Pts',(-26.847438158004,25.6943271445881,-46.1437866326871));
#56728=CARTESIAN_POINT('Ctrl Pts',(-26.9104292608357,25.5974586132444,-46.1379236699316));
#56729=CARTESIAN_POINT('Ctrl Pts',(-26.9692382243808,25.4976728461835,-46.1320607071761));
#56730=CARTESIAN_POINT('Ctrl Pts',(-27.0235853347113,25.3953672271767,-46.1261977444206));
#56731=CARTESIAN_POINT('Ctrl Pts',(-27.0778766835601,25.2931665762696,-46.1203407972101));
#56732=CARTESIAN_POINT('Ctrl Pts',(-27.1277150893714,25.1884515763986,-46.1144838499996));
#56733=CARTESIAN_POINT('Ctrl Pts',(-27.1728644158078,25.0816480185228,-46.1086269027892));
#56734=CARTESIAN_POINT('Ctrl Pts',(-27.2179783370944,24.9749282137452,-46.1027745484732));
#56735=CARTESIAN_POINT('Ctrl Pts',(-27.2584103323726,24.8661234873855,-46.0969221941572));
#56736=CARTESIAN_POINT('Ctrl Pts',(-27.2939707877688,24.7556830021626,-46.0910698398412));
#56737=CARTESIAN_POINT('Ctrl Pts',(-27.3295141448012,24.6452956195104,-46.0852202994848));
#56738=CARTESIAN_POINT('Ctrl Pts',(-27.3601904933446,24.5332744343669,-46.0793707591284));
#56739=CARTESIAN_POINT('Ctrl Pts',(-27.3858590643831,24.4200867264661,-46.073521218772));
#56740=CARTESIAN_POINT('Ctrl Pts',(-27.4115202849672,24.3069314310076,-46.0676733534905));
#56741=CARTESIAN_POINT('Ctrl Pts',(-27.4321764924474,24.1926106805289,-46.061825488209));
#56742=CARTESIAN_POINT('Ctrl Pts',(-27.4477375135206,24.0776042325897,-46.0559776229274));
#56743=CARTESIAN_POINT('Ctrl Pts',(-27.4633012898499,23.9625774214487,-46.0501287222148));
#56744=CARTESIAN_POINT('Ctrl Pts',(-27.4737680202745,23.8468650794797,-46.0442798215021));
#56745=CARTESIAN_POINT('Ctrl Pts',(-27.4790991777868,23.7309540299923,-46.0384309207894));
#56746=CARTESIAN_POINT('Ctrl Pts',(-27.4819148614464,23.6697348956372,-46.0353417878712));
#56747=CARTESIAN_POINT('Ctrl Pts',(-27.4832988550031,23.6084604087577,-46.0322526549529));
#56748=CARTESIAN_POINT('Ctrl Pts',(-27.4832513490189,23.5472024624234,-46.0291635220347));
#56749=CARTESIAN_POINT('',(-27.4893096392136,23.5490465589118,-44.7791635220347));
#56750=CARTESIAN_POINT('Ctrl Pts',(-27.4794900392396,23.5471764562959,-46.0291620620995));
#56751=CARTESIAN_POINT('Ctrl Pts',(-27.482652033486,23.1070280463571,-46.006945021155));
#56752=CARTESIAN_POINT('Ctrl Pts',(-27.2110024468889,21.3572725754213,-45.9184323430858));
#56753=CARTESIAN_POINT('Ctrl Pts',(-24.6381755688857,19.0272917428667,-45.7636240278909));
#56754=CARTESIAN_POINT('Ctrl Pts',(-20.3330782546349,20.190112578786,-45.5647371165163));
#56755=CARTESIAN_POINT('Ctrl Pts',(-18.9842913296047,24.4406171385372,-45.3658502051413));
#56756=CARTESIAN_POINT('Ctrl Pts',(-21.831235619625,27.8729521150715,-45.1669632937664));
#56757=CARTESIAN_POINT('Ctrl Pts',(-26.1838140696498,27.3421172137652,-44.9714010660644));
#56758=CARTESIAN_POINT('Ctrl Pts',(-27.4843286353731,24.7885886070499,-44.842134475487));
#56759=CARTESIAN_POINT('Ctrl Pts',(-27.4893096392136,23.5490465589118,-44.7791635220347));
#56760=CARTESIAN_POINT('',(-27.4831640504939,23.5538871935688,-43.5291635220347));
#56761=CARTESIAN_POINT('Ctrl Pts',(-27.4893096392136,23.5490465589118,-44.7791635220347));
#56762=CARTESIAN_POINT('Ctrl Pts',(-27.4895726217672,23.4836023345022,-44.775838838362));
#56763=CARTESIAN_POINT('Ctrl Pts',(-27.4880834946516,23.4181703317586,-44.7725141546893));
#56764=CARTESIAN_POINT('Ctrl Pts',(-27.4194264635282,22.0498761014208,-44.7028938338917));
#56765=CARTESIAN_POINT('Ctrl Pts',(-25.8655406100273,19.5153805453182,-44.5703025596418));
#56766=CARTESIAN_POINT('Ctrl Pts',(-21.4071583898454,19.4213424659167,-44.3714156482669));
#56767=CARTESIAN_POINT('Ctrl Pts',(-18.9180979816037,23.1214226631191,-44.1725287368921));
#56768=CARTESIAN_POINT('Ctrl Pts',(-20.685594862955,27.2155611507664,-43.9736418255171));
#56769=CARTESIAN_POINT('Ctrl Pts',(-25.0854692589609,27.9415917844081,-43.7747549141422));
#56770=CARTESIAN_POINT('Ctrl Pts',(-27.3122087991913,25.4763978711854,-43.6265954796481));
#56771=CARTESIAN_POINT('Ctrl Pts',(-27.4860063149194,23.8615827651834,-43.5447316822789));
#56772=CARTESIAN_POINT('Ctrl Pts',(-27.4831640504939,23.5538871935688,-43.5291635220347));
#56773=CARTESIAN_POINT('',(-27.4767710526401,23.5498218007742,-42.2791635220347));
#56774=CARTESIAN_POINT('Ctrl Pts',(-27.4831640504939,23.5538871935688,-43.5291635220347));
#56775=CARTESIAN_POINT('Ctrl Pts',(-27.4739027825809,22.5512883154403,-43.4784360451539));
#56776=CARTESIAN_POINT('Ctrl Pts',(-26.5733994698775,20.2236067000968,-43.3614129311482));
#56777=CARTESIAN_POINT('Ctrl Pts',(-22.6540126249395,18.9854409406596,-43.1780941800175));
#56778=CARTESIAN_POINT('Ctrl Pts',(-19.2253442867124,21.8368000215273,-42.9792072686427));
#56779=CARTESIAN_POINT('Ctrl Pts',(-19.7708999338745,26.2626766824239,-42.7803203572679));
#56780=CARTESIAN_POINT('Ctrl Pts',(-23.789360182175,28.1960655244424,-42.5814334458929));
#56781=CARTESIAN_POINT('Ctrl Pts',(-26.9800591897039,26.2342106968784,-42.414381167482));
#56782=CARTESIAN_POINT('Ctrl Pts',(-27.4761053845458,24.2337235905629,-42.3136245261958));
#56783=CARTESIAN_POINT('Ctrl Pts',(-27.4767710526401,23.5498218007742,-42.2791635220347));
#56784=CARTESIAN_POINT('',(-27.4832509871795,23.5467669685326,-41.0291635220347));
#56785=CARTESIAN_POINT('Ctrl Pts',(-27.4767710526401,23.5498218007742,-42.2791635220347));
#56786=CARTESIAN_POINT('Ctrl Pts',(-27.4773859882745,22.9180421126532,-42.2473288890708));
#56787=CARTESIAN_POINT('Ctrl Pts',(-27.0347362334315,20.9713941367988,-42.1491986189821));
#56788=CARTESIAN_POINT('Ctrl Pts',(-23.9731208222587,18.9175499467075,-41.9847727117682));
#56789=CARTESIAN_POINT('Ctrl Pts',(-19.8812603560255,20.6903142024657,-41.7858858003934));
#56790=CARTESIAN_POINT('Ctrl Pts',(-19.1608926199949,25.0911193000017,-41.5869988890184));
#56791=CARTESIAN_POINT('Ctrl Pts',(-22.4739744864657,28.0759984814201,-41.3881119776436));
#56792=CARTESIAN_POINT('Ctrl Pts',(-26.4961175464744,26.9784891217487,-41.2021671032004));
#56793=CARTESIAN_POINT('Ctrl Pts',(-27.4750186852402,24.600193314807,-41.0825178658824));
#56794=CARTESIAN_POINT('Ctrl Pts',(-27.4847500155487,23.5467803226292,-41.0291642656893));
#56795=CARTESIAN_POINT('',(-27.4850771999075,23.5522961849479,-39.7791629056863));
#56796=CARTESIAN_POINT('Ctrl Pts',(-27.4832509871795,23.5467669685326,-41.0291635220347));
#56797=CARTESIAN_POINT('Ctrl Pts',(-27.4831016864497,23.3783007803076,-41.0206276628369));
#56798=CARTESIAN_POINT('Ctrl Pts',(-27.4721249776244,23.2102952848097,-41.012091803639));
#56799=CARTESIAN_POINT('Ctrl Pts',(-27.4505169199899,23.0438666102941,-41.0035559444412));
#56800=CARTESIAN_POINT('Ctrl Pts',(-27.4393635511366,22.9579616008736,-40.9991500145921));
#56801=CARTESIAN_POINT('Ctrl Pts',(-27.4253783983837,22.8724761011641,-40.994744084743));
#56802=CARTESIAN_POINT('Ctrl Pts',(-27.4085928781309,22.7875607387275,-40.9903381548939));
#56803=CARTESIAN_POINT('Ctrl Pts',(-27.3862208560891,22.6743841239126,-40.9844658579251));
#56804=CARTESIAN_POINT('Ctrl Pts',(-27.3588274220373,22.5620030992679,-40.9785935609564));
#56805=CARTESIAN_POINT('Ctrl Pts',(-27.326481872693,22.4508977371991,-40.9727212639876));
#56806=CARTESIAN_POINT('Ctrl Pts',(-27.2941782406119,22.3399363588557,-40.9668565770494));
#56807=CARTESIAN_POINT('Ctrl Pts',(-27.2569353699205,22.2302477487934,-40.9609918901112));
#56808=CARTESIAN_POINT('Ctrl Pts',(-27.2148737397359,22.1223028121415,-40.9551272031729));
#56809=CARTESIAN_POINT('Ctrl Pts',(-27.1728553673048,22.0144688900993,-40.949268547698));
#56810=CARTESIAN_POINT('Ctrl Pts',(-27.1260282418908,21.9083754574422,-40.9434098922232));
#56811=CARTESIAN_POINT('Ctrl Pts',(-27.0745627293182,21.8044785970384,-40.9375512367483));
#56812=CARTESIAN_POINT('Ctrl Pts',(-27.0210869284949,21.6965234337574,-40.9314637370304));
#56813=CARTESIAN_POINT('Ctrl Pts',(-26.9626031215471,21.5909403776341,-40.9253762373125));
#56814=CARTESIAN_POINT('Ctrl Pts',(-26.8993578384398,21.488218913072,-40.9192887375946));
#56815=CARTESIAN_POINT('Ctrl Pts',(-26.8385605986392,21.3894735014488,-40.9134368675112));
#56816=CARTESIAN_POINT('Ctrl Pts',(-26.7733638718324,21.2933726573776,-40.9075849974277));
#56817=CARTESIAN_POINT('Ctrl Pts',(-26.7040332397333,21.2003256720664,-40.9017331273442));
#56818=CARTESIAN_POINT('Ctrl Pts',(-26.6347131638534,21.1072928540048,-40.8958821482612));
#56819=CARTESIAN_POINT('Ctrl Pts',(-26.5612606811033,21.0173133015696,-40.8900311691782));
#56820=CARTESIAN_POINT('Ctrl Pts',(-26.4839836208811,20.9307657696856,-40.8841801900952));
#56821=CARTESIAN_POINT('Ctrl Pts',(-26.4066996127076,20.8442104563456,-40.8783286849528));
#56822=CARTESIAN_POINT('Ctrl Pts',(-26.3255906188283,20.7610880853406,-40.8724771798105));
#56823=CARTESIAN_POINT('Ctrl Pts',(-26.2410030356066,20.6817423389817,-40.8666256746681));
#56824=CARTESIAN_POINT('Ctrl Pts',(-26.1563873626897,20.6023702436277,-40.8607722263683));
#56825=CARTESIAN_POINT('Ctrl Pts',(-26.0682911047986,20.526777549353,-40.8549187780685));
#56826=CARTESIAN_POINT('Ctrl Pts',(-25.977095047568,20.4552687832478,-40.8490653297686));
#56827=CARTESIAN_POINT('Ctrl Pts',(-25.8857952806177,20.3836786961478,-40.843205224827));
#56828=CARTESIAN_POINT('Ctrl Pts',(-25.7913890037402,20.3161820623535,-40.8373451198854));
#56829=CARTESIAN_POINT('Ctrl Pts',(-25.6942874742751,20.2530411091445,-40.8314850149438));
#56830=CARTESIAN_POINT('Ctrl Pts',(-25.5971205530072,20.1898576344554,-40.8256209635883));
#56831=CARTESIAN_POINT('Ctrl Pts',(-25.497255120277,20.1310358903768,-40.8197569122328));
#56832=CARTESIAN_POINT('Ctrl Pts',(-25.39512707184,20.0767921632544,-40.8138928608773));
#56833=CARTESIAN_POINT('Ctrl Pts',(-25.2928485070464,20.0224684917063,-40.8080201670807));
#56834=CARTESIAN_POINT('Ctrl Pts',(-25.1883010431383,19.9727364798982,-40.8021474732841));
#56835=CARTESIAN_POINT('Ctrl Pts',(-25.0819406401324,19.9277643621526,-40.7962747794875));
#56836=CARTESIAN_POINT('Ctrl Pts',(-25.05282094099,19.915451748609,-40.7946669341646));
#56837=CARTESIAN_POINT('Ctrl Pts',(-25.0235654344391,19.9034956346859,-40.7930590888417));
#56838=CARTESIAN_POINT('Ctrl Pts',(-24.9941836535463,19.8918988151508,-40.7914512435188));
#56839=CARTESIAN_POINT('Ctrl Pts',(-24.8868732422674,19.8495440144535,-40.7855789465501));
#56840=CARTESIAN_POINT('Ctrl Pts',(-24.7775178882831,19.8118438621452,-40.7797066495814));
#56841=CARTESIAN_POINT('Ctrl Pts',(-24.6665589423767,19.7789995572215,-40.7738343526127));
#56842=CARTESIAN_POINT('Ctrl Pts',(-24.555743790452,19.7461978159086,-40.7679696656745));
#56843=CARTESIAN_POINT('Ctrl Pts',(-24.4433295719789,19.7182395241225,-40.7621049787363));
#56844=CARTESIAN_POINT('Ctrl Pts',(-24.3297775914139,19.6952778649462,-40.7562402917981));
#56845=CARTESIAN_POINT('Ctrl Pts',(-24.2163423919526,19.6723398203989,-40.7503816363233));
#56846=CARTESIAN_POINT('Ctrl Pts',(-24.1017721605685,19.6543882687158,-40.7445229808485));
#56847=CARTESIAN_POINT('Ctrl Pts',(-23.9865426973814,19.6415264103953,-40.7386643253736));
#56848=CARTESIAN_POINT('Ctrl Pts',(-23.8668122698692,19.6281621565601,-40.7325768256557));
#56849=CARTESIAN_POINT('Ctrl Pts',(-23.7463704962939,19.6202934467827,-40.7264893259378));
#56850=CARTESIAN_POINT('Ctrl Pts',(-23.625762447994,19.6179774583378,-40.7204018262199));
#56851=CARTESIAN_POINT('Ctrl Pts',(-23.5098227909313,19.6157511151554,-40.7145499561366));
#56852=CARTESIAN_POINT('Ctrl Pts',(-23.3937299436869,19.61865563508,-40.7086980860532));
#56853=CARTESIAN_POINT('Ctrl Pts',(-23.2779718079965,19.6266888190087,-40.7028462159698));
#56854=CARTESIAN_POINT('Ctrl Pts',(-23.1622312975349,19.634720779812,-40.6969952368868));
#56855=CARTESIAN_POINT('Ctrl Pts',(-23.0468258095748,19.6478798233579,-40.6911442578039));
#56856=CARTESIAN_POINT('Ctrl Pts',(-22.9322403918285,19.6661117007023,-40.6852932787209));
#56857=CARTESIAN_POINT('Ctrl Pts',(-22.8176446717505,19.6843452172678,-40.6794417735786));
#56858=CARTESIAN_POINT('Ctrl Pts',(-22.7038695767311,19.7076524093489,-40.6735902684364));
#56859=CARTESIAN_POINT('Ctrl Pts',(-22.5913914943841,19.7359276227321,-40.6677387632941));
#56860=CARTESIAN_POINT('Ctrl Pts',(-22.4788760605146,19.7642122256982,-40.6618853149943));
#56861=CARTESIAN_POINT('Ctrl Pts',(-22.3676588964537,19.7974680297047,-40.6560318666946));
#56862=CARTESIAN_POINT('Ctrl Pts',(-22.2582020367302,19.8355392832101,-40.6501784183948));
#56863=CARTESIAN_POINT('Ctrl Pts',(-22.148620700789,19.8736538319978,-40.6443183134533));
#56864=CARTESIAN_POINT('Ctrl Pts',(-22.0408040554849,19.9165946247544,-40.6384582085118));
#56865=CARTESIAN_POINT('Ctrl Pts',(-21.9351950190544,19.9641574087414,-40.6325981035702));
#56866=CARTESIAN_POINT('Ctrl Pts',(-21.8295148615476,20.0117522232866,-40.6267340522148));
#56867=CARTESIAN_POINT('Ctrl Pts',(-21.7260456413423,20.0639750411031,-40.6208700008593));
#56868=CARTESIAN_POINT('Ctrl Pts',(-21.6252049439045,20.1205760477171,-40.6150059495039));
#56869=CARTESIAN_POINT('Ctrl Pts',(-21.5242156274085,20.1772604729163,-40.6091332557073));
#56870=CARTESIAN_POINT('Ctrl Pts',(-21.4258629151349,20.2383357477522,-40.6032605619108));
#56871=CARTESIAN_POINT('Ctrl Pts',(-21.3305348111603,20.3035092031959,-40.5973878681142));
#56872=CARTESIAN_POINT('Ctrl Pts',(-21.3044355709357,20.3213526050783,-40.5957800227908));
#56873=CARTESIAN_POINT('Ctrl Pts',(-21.2785628501617,20.3395029671702,-40.5941721774675));
#56874=CARTESIAN_POINT('Ctrl Pts',(-21.25292415315,20.3579537798329,-40.5925643321441));
#56875=CARTESIAN_POINT('Ctrl Pts',(-21.1592845221766,20.425341263998,-40.5866920351754));
#56876=CARTESIAN_POINT('Ctrl Pts',(-21.0684555467662,20.4969652275506,-40.5808197382067));
#56877=CARTESIAN_POINT('Ctrl Pts',(-20.9808450678181,20.572563111258,-40.574947441238));
#56878=CARTESIAN_POINT('Ctrl Pts',(-20.8933481250928,20.648063026112,-40.5690827542998));
#56879=CARTESIAN_POINT('Ctrl Pts',(-20.8090616944605,20.7275263522804,-40.5632180673616));
#56880=CARTESIAN_POINT('Ctrl Pts',(-20.7283640060337,20.8106477885341,-40.5573533804234));
#56881=CARTESIAN_POINT('Ctrl Pts',(-20.6477493101276,20.8936837395941,-40.5514947249486));
#56882=CARTESIAN_POINT('Ctrl Pts',(-20.5707163014611,20.9803700228401,-40.5456360694738));
#56883=CARTESIAN_POINT('Ctrl Pts',(-20.4976089944803,21.0703621238927,-40.539777413999));
#56884=CARTESIAN_POINT('Ctrl Pts',(-20.4216460516966,21.1638693956765,-40.5336899142811));
#56885=CARTESIAN_POINT('Ctrl Pts',(-20.349922089631,21.2609457093743,-40.5276024145631));
#56886=CARTESIAN_POINT('Ctrl Pts',(-20.2827798466498,21.3611633940645,-40.5215149148452));
#56887=CARTESIAN_POINT('Ctrl Pts',(-20.218236487103,21.457501939944,-40.5156630447619));
#56888=CARTESIAN_POINT('Ctrl Pts',(-20.1579270029877,21.5567428163157,-40.5098111746785));
#56889=CARTESIAN_POINT('Ctrl Pts',(-20.1021132757333,21.6584743545547,-40.5039593045951));
#56890=CARTESIAN_POINT('Ctrl Pts',(-20.0463080466263,21.7601904032421,-40.4981083255121));
#56891=CARTESIAN_POINT('Ctrl Pts',(-19.9949974121188,21.8643959974527,-40.4922573464291));
#56892=CARTESIAN_POINT('Ctrl Pts',(-19.948397920515,21.9706537345538,-40.4864063673462));
#56893=CARTESIAN_POINT('Ctrl Pts',(-19.9017942391685,22.076921025248,-40.4805548622039));
#56894=CARTESIAN_POINT('Ctrl Pts',(-19.8599027087935,22.1852404470163,-40.4747033570616));
#56895=CARTESIAN_POINT('Ctrl Pts',(-19.8228919484283,22.2951540963848,-40.4688518519193));
#56896=CARTESIAN_POINT('Ctrl Pts',(-19.7858688975954,22.4051042456837,-40.4629984036195));
#56897=CARTESIAN_POINT('Ctrl Pts',(-19.753729971475,22.5166492837163,-40.4571449553198));
#56898=CARTESIAN_POINT('Ctrl Pts',(-19.7265938829317,22.6293163027706,-40.45129150702));
#56899=CARTESIAN_POINT('Ctrl Pts',(-19.6994269347633,22.7421114486908,-40.4454314020785));
#56900=CARTESIAN_POINT('Ctrl Pts',(-19.6772742767218,22.8560307202338,-40.4395712971369));
#56901=CARTESIAN_POINT('Ctrl Pts',(-19.6602034836346,22.9705910755917,-40.4337111921954));
#56902=CARTESIAN_POINT('Ctrl Pts',(-19.6431211944367,23.0852285801789,-40.4278471408399));
#56903=CARTESIAN_POINT('Ctrl Pts',(-19.6311276273805,23.2005076180819,-40.4219830894845));
#56904=CARTESIAN_POINT('Ctrl Pts',(-19.6242383320048,23.3159418323282,-40.4161190381291));
#56905=CARTESIAN_POINT('Ctrl Pts',(-19.617338883183,23.4315461735634,-40.4102463443325));
#56906=CARTESIAN_POINT('Ctrl Pts',(-19.6155587261871,23.5473057357987,-40.4043736505359));
#56907=CARTESIAN_POINT('Ctrl Pts',(-19.6188613663048,23.6627358846772,-40.3985009567394));
#56908=CARTESIAN_POINT('Ctrl Pts',(-19.6197655739227,23.6943387285313,-40.3968931114159));
#56909=CARTESIAN_POINT('Ctrl Pts',(-19.6210504756811,23.7259169227772,-40.3952852660925));
#56910=CARTESIAN_POINT('Ctrl Pts',(-19.6227146513102,23.757460635176,-40.3936774207691));
#56911=CARTESIAN_POINT('Ctrl Pts',(-19.6287926821754,23.8726670197724,-40.3878051238004));
#56912=CARTESIAN_POINT('Ctrl Pts',(-19.6399542127138,23.9877987493919,-40.3819328268317));
#56913=CARTESIAN_POINT('Ctrl Pts',(-19.6561988027336,24.102370776247,-40.376060529863));
#56914=CARTESIAN_POINT('Ctrl Pts',(-19.6724223410549,24.2167943268545,-40.3701958429248));
#56915=CARTESIAN_POINT('Ctrl Pts',(-19.6937157817035,24.3306592116078,-40.3643311559866));
#56916=CARTESIAN_POINT('Ctrl Pts',(-19.7200267190434,24.4434821909103,-40.3584664690484));
#56917=CARTESIAN_POINT('Ctrl Pts',(-19.7463105972312,24.5561891388413,-40.3526078135735));
#56918=CARTESIAN_POINT('Ctrl Pts',(-19.7776016149248,24.6678559124983,-40.3467491580987));
#56919=CARTESIAN_POINT('Ctrl Pts',(-19.8137958807882,24.7780068621287,-40.3408905026239));
#56920=CARTESIAN_POINT('Ctrl Pts',(-19.8514039265558,24.8924604048713,-40.334803002906));
#56921=CARTESIAN_POINT('Ctrl Pts',(-19.8943060159491,25.0052768404701,-40.3287155031881));
#56922=CARTESIAN_POINT('Ctrl Pts',(-19.942327606863,25.1159366431234,-40.3226280034702));
#56923=CARTESIAN_POINT('Ctrl Pts',(-19.9884904198813,25.2223131225635,-40.3167761333868));
#56924=CARTESIAN_POINT('Ctrl Pts',(-20.0393836013961,25.3266964042356,-40.3109242633034));
#56925=CARTESIAN_POINT('Ctrl Pts',(-20.0948023657008,25.4286436385556,-40.30507239322));
#56926=CARTESIAN_POINT('Ctrl Pts',(-20.1502126919947,25.5305753504823,-40.299221414137));
#56927=CARTESIAN_POINT('Ctrl Pts',(-20.2101470336281,25.6300713894557,-40.293370435054));
#56928=CARTESIAN_POINT('Ctrl Pts',(-20.2743544499655,25.7267131350882,-40.2875194559711));
#56929=CARTESIAN_POINT('Ctrl Pts',(-20.3385676391675,25.8233635697436,-40.2816679508288));
#56930=CARTESIAN_POINT('Ctrl Pts',(-20.4070544380356,25.9171588565667,-40.2758164456865));
#56931=CARTESIAN_POINT('Ctrl Pts',(-20.4795207504331,26.0077096172917,-40.2699649405442));
#56932=CARTESIAN_POINT('Ctrl Pts',(-20.5520111273155,26.0982904479531,-40.2641114922444));
#56933=CARTESIAN_POINT('Ctrl Pts',(-20.628483387309,26.1856242875196,-40.2582580439446));
#56934=CARTESIAN_POINT('Ctrl Pts',(-20.7086038345567,26.2693556342,-40.2524045956448));
#56935=CARTESIAN_POINT('Ctrl Pts',(-20.7888153961507,26.3531822016034,-40.2465444907033));
#56936=CARTESIAN_POINT('Ctrl Pts',(-20.8726831398765,26.4333978001463,-40.2406843857618));
#56937=CARTESIAN_POINT('Ctrl Pts',(-20.9598372016155,26.5096844734177,-40.2348242808202));
#56938=CARTESIAN_POINT('Ctrl Pts',(-21.0470499561602,26.5860225209889,-40.2289602294648));
#56939=CARTESIAN_POINT('Ctrl Pts',(-21.1375531134912,26.6584261171962,-40.2230961781093));
#56940=CARTESIAN_POINT('Ctrl Pts',(-21.230945898512,26.7266192833898,-40.2172321267539));
#56941=CARTESIAN_POINT('Ctrl Pts',(-21.3244763258551,26.7949129526978,-40.2113594329573));
#56942=CARTESIAN_POINT('Ctrl Pts',(-21.420904537484,26.8589835794306,-40.2054867391607));
#56943=CARTESIAN_POINT('Ctrl Pts',(-21.5198030754438,26.9185999017872,-40.1996140453642));
#56944=CARTESIAN_POINT('Ctrl Pts',(-21.5468798407662,26.9349218535889,-40.1980062000409));
#56945=CARTESIAN_POINT('Ctrl Pts',(-21.5741416492813,26.9509101968645,-40.1963983547175));
#56946=CARTESIAN_POINT('Ctrl Pts',(-21.6015794612456,26.9665608117691,-40.1947905093942));
#56947=CARTESIAN_POINT('Ctrl Pts',(-21.7017899589164,27.0237211972432,-40.1889182124255));
#56948=CARTESIAN_POINT('Ctrl Pts',(-21.8046854951808,27.0765643949701,-40.1830459154568));
#56949=CARTESIAN_POINT('Ctrl Pts',(-21.9098577532546,27.1248285863989,-40.1771736184881));
#56950=CARTESIAN_POINT('Ctrl Pts',(-22.0148937164346,27.1730302312686,-40.1713089315499));
#56951=CARTESIAN_POINT('Ctrl Pts',(-22.1222001617944,27.2166644996686,-40.1654442446117));
#56952=CARTESIAN_POINT('Ctrl Pts',(-22.2313422042853,27.2555142698517,-40.1595795576735));
#56953=CARTESIAN_POINT('Ctrl Pts',(-22.340372001018,27.2943240854783,-40.1537209021987));
#56954=CARTESIAN_POINT('Ctrl Pts',(-22.4512332528523,27.3283590523365,-40.1478622467238));
#56955=CARTESIAN_POINT('Ctrl Pts',(-22.5634696299993,27.3574494670947,-40.142003591249));
#56956=CARTESIAN_POINT('Ctrl Pts',(-22.6800900588941,27.3876761790758,-40.1359160915311));
#56957=CARTESIAN_POINT('Ctrl Pts',(-22.7981948170911,27.4125639975166,-40.1298285918132));
#56958=CARTESIAN_POINT('Ctrl Pts',(-22.9172524714096,27.4319789418988,-40.1237410920953));
#56959=CARTESIAN_POINT('Ctrl Pts',(-23.0317017457902,27.4506423895318,-40.1178892220119));
#56960=CARTESIAN_POINT('Ctrl Pts',(-23.1470310741534,27.4642486908902,-40.1120373519285));
#56961=CARTESIAN_POINT('Ctrl Pts',(-23.2627571843576,27.4727307566509,-40.1061854818451));
#56962=CARTESIAN_POINT('Ctrl Pts',(-23.3784656742093,27.48121153094,-40.1003345027621));
#56963=CARTESIAN_POINT('Ctrl Pts',(-23.4945704136167,27.4845695907323,-40.0944835236791));
#56964=CARTESIAN_POINT('Ctrl Pts',(-23.6105835661724,27.4827897745285,-40.0886325445961));
#56965=CARTESIAN_POINT('Ctrl Pts',(-23.7266071494271,27.4810097983021,-40.0827810394538));
#56966=CARTESIAN_POINT('Ctrl Pts',(-23.8425387161017,27.4740910341182,-40.0769295343115));
#56967=CARTESIAN_POINT('Ctrl Pts',(-23.9578917042987,27.4620704345315,-40.0710780291692));
#56968=CARTESIAN_POINT('Ctrl Pts',(-24.0732829987118,27.4500458431654,-40.0652245808694));
#56969=CARTESIAN_POINT('Ctrl Pts',(-24.1880949216634,27.4329160903923,-40.0593711325697));
#56970=CARTESIAN_POINT('Ctrl Pts',(-24.301848006775,27.4107697563466,-40.0535176842699));
#56971=CARTESIAN_POINT('Ctrl Pts',(-24.4157304538454,27.3885982371101,-40.0476575793284));
#56972=CARTESIAN_POINT('Ctrl Pts',(-24.5285512536664,27.3613988287529,-40.0417974743868));
#56973=CARTESIAN_POINT('Ctrl Pts',(-24.6398429769391,27.3293108352443,-40.0359373694453));
#56974=CARTESIAN_POINT('Ctrl Pts',(-24.751209648222,27.2972012324804,-40.0300733180898));
#56975=CARTESIAN_POINT('Ctrl Pts',(-24.8610448017554,27.2601966208898,-40.0242092667343));
#56976=CARTESIAN_POINT('Ctrl Pts',(-24.968899616141,27.2184850011256,-40.0183452153789));
#56977=CARTESIAN_POINT('Ctrl Pts',(-25.0769133869931,27.1767119067603,-40.0124725215823));
#56978=CARTESIAN_POINT('Ctrl Pts',(-25.1829406165239,27.1302181243161,-40.0065998277857));
#56979=CARTESIAN_POINT('Ctrl Pts',(-25.2865556811539,27.0792382745354,-40.0007271339891));
#56980=CARTESIAN_POINT('Ctrl Pts',(-25.3149237525804,27.0652808444546,-39.9991192886659));
#56981=CARTESIAN_POINT('Ctrl Pts',(-25.3431111772467,27.0509874048801,-39.9975114433426));
#56982=CARTESIAN_POINT('Ctrl Pts',(-25.3711096026936,27.0363633341489,-39.9959035980193));
#56983=CARTESIAN_POINT('Ctrl Pts',(-25.4733676162594,26.9829521726515,-39.9900313010506));
#56984=CARTESIAN_POINT('Ctrl Pts',(-25.5734448845254,26.9249484201392,-39.9841590040819));
#56985=CARTESIAN_POINT('Ctrl Pts',(-25.6709004226202,26.8625540763473,-39.9782867071132));
#56986=CARTESIAN_POINT('Ctrl Pts',(-25.7682296660774,26.8002405906696,-39.972422020175));
#56987=CARTESIAN_POINT('Ctrl Pts',(-25.8629435909488,26.7335480496325,-39.9665573332368));
#56988=CARTESIAN_POINT('Ctrl Pts',(-25.9546244552608,26.6627249658155,-39.9606926462986));
#56989=CARTESIAN_POINT('Ctrl Pts',(-26.046211031543,26.5919747191066,-39.9548339908238));
#56990=CARTESIAN_POINT('Ctrl Pts',(-26.1347704265662,26.5171026303126,-39.948975335349));
#56991=CARTESIAN_POINT('Ctrl Pts',(-26.219913200474,26.4384008854964,-39.9431166798742));
#56992=CARTESIAN_POINT('Ctrl Pts',(-26.3083817261235,26.3566249812079,-39.9370291801563));
#56993=CARTESIAN_POINT('Ctrl Pts',(-26.3931608939733,26.2707143874827,-39.9309416804383));
#56994=CARTESIAN_POINT('Ctrl Pts',(-26.4738507218022,26.1810437858224,-39.9248541807204));
#56995=CARTESIAN_POINT('Ctrl Pts',(-26.5514172780876,26.0948440756732,-39.919002310637));
#56996=CARTESIAN_POINT('Ctrl Pts',(-26.6252048788477,26.0051703593938,-39.9131504405537));
#56997=CARTESIAN_POINT('Ctrl Pts',(-26.6948958516298,25.9123929573219,-39.9072985704703));
#56998=CARTESIAN_POINT('Ctrl Pts',(-26.7645762133275,25.819629681453,-39.9014475913873));
#56999=CARTESIAN_POINT('Ctrl Pts',(-26.830160939052,25.7237639898318,-39.8955966123043));
#57000=CARTESIAN_POINT('Ctrl Pts',(-26.8913735769205,25.6251981119796,-39.8897456332214));
#57001=CARTESIAN_POINT('Ctrl Pts',(-26.9525917183942,25.5266233721065,-39.8838941280791));
#57002=CARTESIAN_POINT('Ctrl Pts',(-27.0094367724771,25.4253483145863,-39.8780426229368));
#57003=CARTESIAN_POINT('Ctrl Pts',(-27.0616768206409,25.3218022665295,-39.8721911177945));
#57004=CARTESIAN_POINT('Ctrl Pts',(-27.1139342165874,25.2182218330845,-39.8663376694947));
#57005=CARTESIAN_POINT('Ctrl Pts',(-27.1615833797504,25.1123692784073,-39.860484221195));
#57006=CARTESIAN_POINT('Ctrl Pts',(-27.2044396621794,25.0046958669246,-39.8546307728952));
#57007=CARTESIAN_POINT('Ctrl Pts',(-27.2473446815077,24.8969000073919,-39.8487706679537));
#57008=CARTESIAN_POINT('Ctrl Pts',(-27.2854457880149,24.7872795422856,-39.8429105630122));
#57009=CARTESIAN_POINT('Ctrl Pts',(-27.3186075151159,24.6763030274185,-39.8370504580706));
#57010=CARTESIAN_POINT('Ctrl Pts',(-27.3517915745645,24.5652517768145,-39.8311864067152));
#57011=CARTESIAN_POINT('Ctrl Pts',(-27.3800295306883,24.4528430580043,-39.8253223553598));
#57012=CARTESIAN_POINT('Ctrl Pts',(-27.4032369445985,24.3395560942837,-39.8194583040043));
#57013=CARTESIAN_POINT('Ctrl Pts',(-27.4264785616041,24.2261021681927,-39.8135856102078));
#57014=CARTESIAN_POINT('Ctrl Pts',(-27.4446747747246,24.1117678206154,-39.8077129164112));
#57015=CARTESIAN_POINT('Ctrl Pts',(-27.4577929067385,23.9970379582675,-39.8018402226146));
#57016=CARTESIAN_POINT('Ctrl Pts',(-27.4613844318446,23.9656268411517,-39.8002323772912));
#57017=CARTESIAN_POINT('Ctrl Pts',(-27.4645956192938,23.9341860778103,-39.7986245319678));
#57018=CARTESIAN_POINT('Ctrl Pts',(-27.4674264791132,23.9027256025266,-39.7970166866444));
#57019=CARTESIAN_POINT('Ctrl Pts',(-27.4779042295962,23.7862821785711,-39.7910656317745));
#57020=CARTESIAN_POINT('Ctrl Pts',(-27.4831908370144,23.6693646861602,-39.7851145769046));
#57021=CARTESIAN_POINT('Ctrl Pts',(-27.4832519949075,23.5523073708991,-39.7791635220347));
#57022=CARTESIAN_POINT('',(-27.4815728590188,23.5527517371402,-38.5291640444444));
#57023=CARTESIAN_POINT('Ctrl Pts',(-27.4884312052316,23.5522756295914,-39.7791617730815));
#57024=CARTESIAN_POINT('Ctrl Pts',(-27.4808809331833,22.3637409737853,-39.7188177738108));
#57025=CARTESIAN_POINT('Ctrl Pts',(-26.273746231481,19.8561955596585,-39.5921781374153));
#57026=CARTESIAN_POINT('Ctrl Pts',(-22.0037382742824,19.1628792305343,-39.3992428638946));
#57027=CARTESIAN_POINT('Ctrl Pts',(-19.0231252434711,22.4797996610202,-39.2003559525198));
#57028=CARTESIAN_POINT('Ctrl Pts',(-20.2025583534408,26.7803755202187,-39.0014690411448));
#57029=CARTESIAN_POINT('Ctrl Pts',(-24.4582385755645,28.1127422222292,-38.80258212977));
#57030=CARTESIAN_POINT('Ctrl Pts',(-27.1664814591117,25.8486886819478,-38.6451474635765));
#57031=CARTESIAN_POINT('Ctrl Pts',(-27.4811981277005,24.0453033749675,-38.554008434508));
#57032=CARTESIAN_POINT('Ctrl Pts',(-27.4783651688805,23.5527694946165,-38.5291650425645));
#57033=CARTESIAN_POINT('',(-27.4820553179501,23.5472580460612,-37.2791630686818));
#57034=CARTESIAN_POINT('Ctrl Pts',(-27.4832517435352,23.5527424429907,-38.5291635220347));
#57035=CARTESIAN_POINT('Ctrl Pts',(-27.4833258207743,23.4357319600559,-38.523268827156));
#57036=CARTESIAN_POINT('Ctrl Pts',(-27.4781738034219,23.318699749024,-38.5173741322774));
#57037=CARTESIAN_POINT('Ctrl Pts',(-27.4678164922244,23.202141033529,-38.5114794373987));
#57038=CARTESIAN_POINT('Ctrl Pts',(-27.4574581828925,23.0855710852667,-38.5055841744481));
#57039=CARTESIAN_POINT('Ctrl Pts',(-27.4418936169437,22.9694751265147,-38.4996889114975));
#57040=CARTESIAN_POINT('Ctrl Pts',(-27.4211954988383,22.8543433816485,-38.4937936485469));
#57041=CARTESIAN_POINT('Ctrl Pts',(-27.4004906542045,22.7391742209672,-38.4878964697383));
#57042=CARTESIAN_POINT('Ctrl Pts',(-27.3746490092089,22.6249702959038,-38.4819992909298));
#57043=CARTESIAN_POINT('Ctrl Pts',(-27.3437942984983,22.5122111724446,-38.4761021121212));
#57044=CARTESIAN_POINT('Ctrl Pts',(-27.3127095232854,22.3986112739134,-38.4701609616962));
#57045=CARTESIAN_POINT('Ctrl Pts',(-27.2765367268469,22.2864782137126,-38.4642198112711));
#57046=CARTESIAN_POINT('Ctrl Pts',(-27.2354529487445,22.1762849606895,-38.458278660846));
#57047=CARTESIAN_POINT('Ctrl Pts',(-27.1945948460353,22.0666970051065,-38.4523701454784));
#57048=CARTESIAN_POINT('Ctrl Pts',(-27.1488797994331,21.9590279468057,-38.4464616301107));
#57049=CARTESIAN_POINT('Ctrl Pts',(-27.0985291928668,21.8537202638673,-38.4405531147431));
#57050=CARTESIAN_POINT('Ctrl Pts',(-27.0477614269543,21.7475400972161,-38.4345956467893));
#57051=CARTESIAN_POINT('Ctrl Pts',(-26.99228114698,21.6437609777045,-38.4286381788355));
#57052=CARTESIAN_POINT('Ctrl Pts',(-26.9323605244277,21.5428077564916,-38.4226807108817));
#57053=CARTESIAN_POINT('Ctrl Pts',(-26.8724399018754,21.4418545352787,-38.4167232429279));
#57054=CARTESIAN_POINT('Ctrl Pts',(-26.8080792180531,21.3437275234703,-38.4107657749741));
#57055=CARTESIAN_POINT('Ctrl Pts',(-26.7395921569827,21.2488178151392,-38.4048083070203));
#57056=CARTESIAN_POINT('Ctrl Pts',(-26.6720842216924,21.1552649841621,-38.3989360100516));
#57057=CARTESIAN_POINT('Ctrl Pts',(-26.6003434276182,21.0645282584402,-38.3930637130829));
#57058=CARTESIAN_POINT('Ctrl Pts',(-26.5246328586346,20.9770151406419,-38.3871914161142));
#57059=CARTESIAN_POINT('Ctrl Pts',(-26.4490204045356,20.889615432894,-38.3813267291759));
#57060=CARTESIAN_POINT('Ctrl Pts',(-26.3694486740837,20.8054313351828,-38.3754620422377));
#57061=CARTESIAN_POINT('Ctrl Pts',(-26.286223455008,20.7248406844087,-38.3695973552995));
#57062=CARTESIAN_POINT('Ctrl Pts',(-26.2030838278604,20.6443329160741,-38.3637386998247));
#57063=CARTESIAN_POINT('Ctrl Pts',(-26.1162984809027,20.567411529707,-38.3578800443499));
#57064=CARTESIAN_POINT('Ctrl Pts',(-26.026212370949,20.4944200961053,-38.3520213888751));
#57065=CARTESIAN_POINT('Ctrl Pts',(-25.9326074181935,20.418577552817,-38.3459338891572));
#57066=CARTESIAN_POINT('Ctrl Pts',(-25.8354388817183,20.3469785798161,-38.3398463894393));
#57067=CARTESIAN_POINT('Ctrl Pts',(-25.7351348731684,20.2799653648059,-38.3337588897214));
#57068=CARTESIAN_POINT('Ctrl Pts',(-25.6387133447776,20.2155460389277,-38.327907019638));
#57069=CARTESIAN_POINT('Ctrl Pts',(-25.5393949369666,20.1553643200487,-38.3220551495546));
#57070=CARTESIAN_POINT('Ctrl Pts',(-25.4375916550404,20.099681559596,-38.3162032794712));
#57071=CARTESIAN_POINT('Ctrl Pts',(-25.3358038735896,20.0440072773499,-38.3103523003882));
#57072=CARTESIAN_POINT('Ctrl Pts',(-25.2315323328709,19.992830789833,-38.3045013213052));
#57073=CARTESIAN_POINT('Ctrl Pts',(-25.1252147138359,19.946368082267,-38.2986503422222));
#57074=CARTESIAN_POINT('Ctrl Pts',(-25.0188875358238,19.8999011972564,-38.2927988370799));
#57075=CARTESIAN_POINT('Ctrl Pts',(-24.9105142926091,19.8581491002485,-38.2869473319376));
#57076=CARTESIAN_POINT('Ctrl Pts',(-24.8005531042859,19.8212798208559,-38.2810958267953));
#57077=CARTESIAN_POINT('Ctrl Pts',(-24.6905554002461,19.7843982979783,-38.2752423784956));
#57078=CARTESIAN_POINT('Ctrl Pts',(-24.5789690942821,19.7524029482666,-38.2693889301958));
#57079=CARTESIAN_POINT('Ctrl Pts',(-24.4662672464887,19.7254118758917,-38.263535481896));
#57080=CARTESIAN_POINT('Ctrl Pts',(-24.3534372322211,19.6983901088063,-38.2576753769545));
#57081=CARTESIAN_POINT('Ctrl Pts',(-24.2394895462633,19.676384074358,-38.2518152720129));
#57082=CARTESIAN_POINT('Ctrl Pts',(-24.1249073169867,19.6594607256809,-38.2459551670714));
#57083=CARTESIAN_POINT('Ctrl Pts',(-24.0102479237504,19.6425259801876,-38.2400911157159));
#57084=CARTESIAN_POINT('Ctrl Pts',(-23.8949535465194,19.6306807782257,-38.2342270643605));
#57085=CARTESIAN_POINT('Ctrl Pts',(-23.7795105618746,19.6239400434175,-38.228363013005));
#57086=CARTESIAN_POINT('Ctrl Pts',(-23.6638974373149,19.6171893741117,-38.2224903192084));
#57087=CARTESIAN_POINT('Ctrl Pts',(-23.5481356800144,19.61555819215,-38.2166176254119));
#57088=CARTESIAN_POINT('Ctrl Pts',(-23.4327098769627,19.6190093791636,-38.2107449316153));
#57089=CARTESIAN_POINT('Ctrl Pts',(-23.4011082229252,19.6199542564366,-38.209137086292));
#57090=CARTESIAN_POINT('Ctrl Pts',(-23.3695317083993,19.6212797958127,-38.2075292409686));
#57091=CARTESIAN_POINT('Ctrl Pts',(-23.337990163788,19.62298456437,-38.2059213956453));
#57092=CARTESIAN_POINT('Ctrl Pts',(-23.2227916965455,19.6292108518654,-38.2000490986766));
#57093=CARTESIAN_POINT('Ctrl Pts',(-23.1076744262871,19.6405205387493,-38.1941768017079));
#57094=CARTESIAN_POINT('Ctrl Pts',(-22.9931233998321,19.6569125606115,-38.1883045047392));
#57095=CARTESIAN_POINT('Ctrl Pts',(-22.8787208224101,19.6732833397151,-38.182439817801));
#57096=CARTESIAN_POINT('Ctrl Pts',(-22.76488343495,19.6947232979882,-38.1765751308628));
#57097=CARTESIAN_POINT('Ctrl Pts',(-22.6520944092062,19.7211794079463,-38.1707104439246));
#57098=CARTESIAN_POINT('Ctrl Pts',(-22.5394213799146,19.7476083094514,-38.1648517884498));
#57099=CARTESIAN_POINT('Ctrl Pts',(-22.4277949678349,19.7790430076925,-38.1589931329749));
#57100=CARTESIAN_POINT('Ctrl Pts',(-22.317690688626,19.8153789992955,-38.1531344775001));
#57101=CARTESIAN_POINT('Ctrl Pts',(-22.2032856392926,19.8531343067348,-38.1470469777822));
#57102=CARTESIAN_POINT('Ctrl Pts',(-22.0905245087702,19.8961815465863,-38.1409594780643));
#57103=CARTESIAN_POINT('Ctrl Pts',(-21.9799265978079,19.9443455082999,-38.1348719783464));
#57104=CARTESIAN_POINT('Ctrl Pts',(-21.8736096144094,19.9906451813531,-38.129020108263));
#57105=CARTESIAN_POINT('Ctrl Pts',(-21.7692919147448,20.041672653895,-38.1231682381796));
#57106=CARTESIAN_POINT('Ctrl Pts',(-21.6674160844884,20.0972225704756,-38.1173163680962));
#57107=CARTESIAN_POINT('Ctrl Pts',(-21.5655557657533,20.1527640290764,-38.1114653890132));
#57108=CARTESIAN_POINT('Ctrl Pts',(-21.4661369400108,20.2128263647485,-38.1056144099302));
#57109=CARTESIAN_POINT('Ctrl Pts',(-21.3695779043605,20.2771580983325,-38.0997634308473));
#57110=CARTESIAN_POINT('Ctrl Pts',(-21.2730101871237,20.3414956159585,-38.093911925705));
#57111=CARTESIAN_POINT('Ctrl Pts',(-21.1793031151586,20.4101030653583,-38.0880604205627));
#57112=CARTESIAN_POINT('Ctrl Pts',(-21.0888456879293,20.4826858495392,-38.0822089154204));
#57113=CARTESIAN_POINT('Ctrl Pts',(-20.9983582217579,20.5552927368825,-38.0763554671206));
#57114=CARTESIAN_POINT('Ctrl Pts',(-20.9111228683668,20.6318773254143,-38.0705020188208));
#57115=CARTESIAN_POINT('Ctrl Pts',(-20.8274946998121,20.712105462051,-38.0646485705211));
#57116=CARTESIAN_POINT('Ctrl Pts',(-20.7437714278701,20.7924248355003,-38.0587884655795));
#57117=CARTESIAN_POINT('Ctrl Pts',(-20.6636638270207,20.8763957410175,-38.052928360638));
#57118=CARTESIAN_POINT('Ctrl Pts',(-20.5874893774252,20.963647905605,-38.0470682556965));
#57119=CARTESIAN_POINT('Ctrl Pts',(-20.5112636291053,21.0509588290646,-38.041204204341));
#57120=CARTESIAN_POINT('Ctrl Pts',(-20.4389765633839,21.1415550892527,-38.0353401529856));
#57121=CARTESIAN_POINT('Ctrl Pts',(-20.3709036429159,21.2350355562416,-38.0294761016301));
#57122=CARTESIAN_POINT('Ctrl Pts',(-20.3027303965518,21.3286537947782,-38.0236034078335));
#57123=CARTESIAN_POINT('Ctrl Pts',(-20.238783918489,21.4251643804734,-38.017730714037));
#57124=CARTESIAN_POINT('Ctrl Pts',(-20.179294920232,21.5241395581103,-38.0118580202404));
#57125=CARTESIAN_POINT('Ctrl Pts',(-20.1630078276387,21.5512373060946,-38.0102501749171));
#57126=CARTESIAN_POINT('Ctrl Pts',(-20.1470545814315,21.57851966779,-38.0086423295938));
#57127=CARTESIAN_POINT('Ctrl Pts',(-20.1314392898184,21.6059775981587,-38.0070344842704));
#57128=CARTESIAN_POINT('Ctrl Pts',(-20.0744079148003,21.7062615738204,-38.0011621873017));
#57129=CARTESIAN_POINT('Ctrl Pts',(-20.0216971793903,21.809225029967,-37.995289890333));
#57130=CARTESIAN_POINT('Ctrl Pts',(-19.9735683764508,21.9144593132125,-37.9894175933643));
#57131=CARTESIAN_POINT('Ctrl Pts',(-19.9255019446175,22.0195572211844,-37.9835529064261));
#57132=CARTESIAN_POINT('Ctrl Pts',(-19.882005807406,22.1269197315975,-37.9776882194879));
#57133=CARTESIAN_POINT('Ctrl Pts',(-19.8432965267201,22.2361116803443,-37.9718235325497));
#57134=CARTESIAN_POINT('Ctrl Pts',(-19.8046270561062,22.3451913320073,-37.9659648770749));
#57135=CARTESIAN_POINT('Ctrl Pts',(-19.7707347872471,22.456096292396,-37.9601062216001));
#57136=CARTESIAN_POINT('Ctrl Pts',(-19.7417888360728,22.5683700137045,-37.9542475661253));
#57137=CARTESIAN_POINT('Ctrl Pts',(-19.7117122305504,22.6850292454569,-37.9481600664074));
#57138=CARTESIAN_POINT('Ctrl Pts',(-19.6869764243636,22.8031659345413,-37.9420725666895));
#57139=CARTESIAN_POINT('Ctrl Pts',(-19.6677147140067,22.9222484757945,-37.9359850669716));
#57140=CARTESIAN_POINT('Ctrl Pts',(-19.6491985691499,23.0367216738079,-37.9301331968882));
#57141=CARTESIAN_POINT('Ctrl Pts',(-19.635740698941,23.1520684169209,-37.9242813268048));
#57142=CARTESIAN_POINT('Ctrl Pts',(-19.6274075707139,23.2678053470534,-37.9184294567214));
#57143=CARTESIAN_POINT('Ctrl Pts',(-19.6190757112813,23.3835246551859,-37.9125784776384));
#57144=CARTESIAN_POINT('Ctrl Pts',(-19.615867072046,23.4996336200104,-37.9067274985554));
#57145=CARTESIAN_POINT('Ctrl Pts',(-19.6177961866868,23.6156443860121,-37.9008765194725));
#57146=CARTESIAN_POINT('Ctrl Pts',(-19.6197254747736,23.7316655824983,-37.8950250143302));
#57147=CARTESIAN_POINT('Ctrl Pts',(-19.6267934281445,23.8475881492598,-37.8891735091879));
#57148=CARTESIAN_POINT('Ctrl Pts',(-19.6389624681078,23.9629255723573,-37.8833220040456));
#57149=CARTESIAN_POINT('Ctrl Pts',(-19.6511355491443,24.078301296502,-37.8774685557458));
#57150=CARTESIAN_POINT('Ctrl Pts',(-19.6684130417542,24.1930910797191,-37.871615107446));
#57151=CARTESIAN_POINT('Ctrl Pts',(-19.6907057488406,24.3068155700227,-37.8657616591463));
#57152=CARTESIAN_POINT('Ctrl Pts',(-19.7130238075758,24.4206693897666,-37.8599015542047));
#57153=CARTESIAN_POINT('Ctrl Pts',(-19.7403683850107,24.5334550926377,-37.8540414492632));
#57154=CARTESIAN_POINT('Ctrl Pts',(-19.772599575746,24.6447054289975,-37.8481813443216));
#57155=CARTESIAN_POINT('Ctrl Pts',(-19.8048524721711,24.7560306854963,-37.8423172929662));
#57156=CARTESIAN_POINT('Ctrl Pts',(-19.8419984024251,24.8658181260177,-37.8364532416107));
#57157=CARTESIAN_POINT('Ctrl Pts',(-19.8838487884123,24.9736191714777,-37.8305891902552));
#57158=CARTESIAN_POINT('Ctrl Pts',(-19.9257608535142,25.0815790941592,-37.8247164964587));
#57159=CARTESIAN_POINT('Ctrl Pts',(-19.9723910462615,25.1875464020056,-37.8188438026621));
#57160=CARTESIAN_POINT('Ctrl Pts',(-20.0235041983619,25.2910957737288,-37.8129711088655));
#57161=CARTESIAN_POINT('Ctrl Pts',(-20.0374981243883,25.3194458595371,-37.8113632635422));
#57162=CARTESIAN_POINT('Ctrl Pts',(-20.0518278271519,25.3476148663168,-37.8097554182189));
#57163=CARTESIAN_POINT('Ctrl Pts',(-20.066487917571,25.375594448537,-37.8081475728955));
#57164=CARTESIAN_POINT('Ctrl Pts',(-20.1200306329556,25.4777836414108,-37.8022752759268));
#57165=CARTESIAN_POINT('Ctrl Pts',(-20.1781631291024,25.5777861804829,-37.7964029789581));
#57166=CARTESIAN_POINT('Ctrl Pts',(-20.24068283893,25.675161341205,-37.7905306819894));
#57167=CARTESIAN_POINT('Ctrl Pts',(-20.303121528179,25.7724103114523,-37.7846659950512));
#57168=CARTESIAN_POINT('Ctrl Pts',(-20.3699359034493,25.8670383297756,-37.778801308113));
#57169=CARTESIAN_POINT('Ctrl Pts',(-20.440876914766,25.9586279743635,-37.7729366211748));
#57170=CARTESIAN_POINT('Ctrl Pts',(-20.5117449676936,26.0501234247356,-37.7670779657));
#57171=CARTESIAN_POINT('Ctrl Pts',(-20.586730963546,26.138586391865,-37.7612193102251));
#57172=CARTESIAN_POINT('Ctrl Pts',(-20.6655422153237,26.2236278122385,-37.7553606547503));
#57173=CARTESIAN_POINT('Ctrl Pts',(-20.7474319040116,26.3119910253952,-37.7492731550324));
#57174=CARTESIAN_POINT('Ctrl Pts',(-20.8334515307957,26.3966595627834,-37.7431856553145));
#57175=CARTESIAN_POINT('Ctrl Pts',(-20.9232258997385,26.4772339246989,-37.7370981555966));
#57176=CARTESIAN_POINT('Ctrl Pts',(-21.0095253606368,26.554689484425,-37.7312462855132));
#57177=CARTESIAN_POINT('Ctrl Pts',(-21.0992939615664,26.6283616209793,-37.7253944154298));
#57178=CARTESIAN_POINT('Ctrl Pts',(-21.1921609736767,26.6979331387455,-37.7195425453464));
#57179=CARTESIAN_POINT('Ctrl Pts',(-21.2850138459401,26.7674940636155,-37.7136915662634));
#57180=CARTESIAN_POINT('Ctrl Pts',(-21.3809638606217,26.8329553633358,-37.7078405871804));
#57181=CARTESIAN_POINT('Ctrl Pts',(-21.4796084327609,26.8940411038908,-37.7019896080974));
#57182=CARTESIAN_POINT('Ctrl Pts',(-21.5782618739963,26.9551323366416,-37.6961381029551));
#57183=CARTESIAN_POINT('Ctrl Pts',(-21.6796100028192,27.0118470105239,-37.6902865978128));
#57184=CARTESIAN_POINT('Ctrl Pts',(-21.7832231940134,27.0639537597122,-37.6844350926705));
#57185=CARTESIAN_POINT('Ctrl Pts',(-21.8868707928928,27.1160778124176,-37.6785816443707));
#57186=CARTESIAN_POINT('Ctrl Pts',(-21.9927845806855,27.163590712112,-37.6727281960709));
#57187=CARTESIAN_POINT('Ctrl Pts',(-22.100513055711,27.2063083917401,-37.6668747477712));
#57188=CARTESIAN_POINT('Ctrl Pts',(-22.2083640414052,27.2490746506458,-37.6610146428296));
#57189=CARTESIAN_POINT('Ctrl Pts',(-22.3180334488997,27.2870346525829,-37.6551545378881));
#57190=CARTESIAN_POINT('Ctrl Pts',(-22.4290525484346,27.3200535340733,-37.6492944329465));
#57191=CARTESIAN_POINT('Ctrl Pts',(-22.5401464123844,27.3530946517138,-37.6434303815911));
#57192=CARTESIAN_POINT('Ctrl Pts',(-22.6525913781656,27.3811879231691,-37.6375663302356));
#57193=CARTESIAN_POINT('Ctrl Pts',(-22.7659081142131,27.4042495263435,-37.6317022788802));
#57194=CARTESIAN_POINT('Ctrl Pts',(-22.8793918565097,27.4273451177176,-37.6258295850836));
#57195=CARTESIAN_POINT('Ctrl Pts',(-22.9937495265209,27.4453941763504,-37.619956891287));
#57196=CARTESIAN_POINT('Ctrl Pts',(-23.1084961758793,27.458364649085,-37.6140841974904));
#57197=CARTESIAN_POINT('Ctrl Pts',(-23.1399118889956,27.4619157475502,-37.6124763521672));
#57198=CARTESIAN_POINT('Ctrl Pts',(-23.1713567588479,27.4650864705212,-37.6108685068439));
#57199=CARTESIAN_POINT('Ctrl Pts',(-23.202820851174,27.4678768408095,-37.6092606615206));
#57200=CARTESIAN_POINT('Ctrl Pts',(-23.3177364411962,27.4780680468591,-37.6033883645519));
#57201=CARTESIAN_POINT('Ctrl Pts',(-23.4332933337633,27.4832158142665,-37.5975160675832));
#57202=CARTESIAN_POINT('Ctrl Pts',(-23.5490112438236,27.4832523358137,-37.5916437706145));
#57203=CARTESIAN_POINT('Ctrl Pts',(-23.6645791926627,27.483288810032,-37.5857790836763));
#57204=CARTESIAN_POINT('Ctrl Pts',(-23.7803073344661,27.4782272105591,-37.5799143967381));
#57205=CARTESIAN_POINT('Ctrl Pts',(-23.895709863191,27.468051433133,-37.5740497098));
#57206=CARTESIAN_POINT('Ctrl Pts',(-24.0109937076391,27.457886120857,-37.5681910543252));
#57207=CARTESIAN_POINT('Ctrl Pts',(-24.1259521957782,27.4426171283577,-37.5623323988503));
#57208=CARTESIAN_POINT('Ctrl Pts',(-24.2400997922157,27.4222803927963,-37.5564737433755));
#57209=CARTESIAN_POINT('Ctrl Pts',(-24.3587060943105,27.4011492864314,-37.5503862436576));
#57210=CARTESIAN_POINT('Ctrl Pts',(-24.4764364103125,27.3745464649719,-37.5442987439397));
#57211=CARTESIAN_POINT('Ctrl Pts',(-24.5927518251079,27.3425716405288,-37.5382112442218));
#57212=CARTESIAN_POINT('Ctrl Pts',(-24.7045650041831,27.3118344697278,-37.5323593741384));
#57213=CARTESIAN_POINT('Ctrl Pts',(-24.8150703431188,27.2761335525973,-37.526507504055));
#57214=CARTESIAN_POINT('Ctrl Pts',(-24.923800585261,27.235609331862,-37.5206556339717));
#57215=CARTESIAN_POINT('Ctrl Pts',(-25.0325142722349,27.1950912813079,-37.5148046548887));
#57216=CARTESIAN_POINT('Ctrl Pts',(-25.13945301256,27.149751531684,-37.5089536758058));
#57217=CARTESIAN_POINT('Ctrl Pts',(-25.2441670440814,27.099779630439,-37.5031026967228));
#57218=CARTESIAN_POINT('Ctrl Pts',(-25.3488904904021,27.0498032362392,-37.4972511915805));
#57219=CARTESIAN_POINT('Ctrl Pts',(-25.4513884571926,26.9951940405561,-37.4913996864383));
#57220=CARTESIAN_POINT('Ctrl Pts',(-25.5512340618596,26.9361884312553,-37.485548181296));
#57221=CARTESIAN_POINT('Ctrl Pts',(-25.6511128230791,26.8771632274758,-37.4796947329962));
#57222=CARTESIAN_POINT('Ctrl Pts',(-25.7483371150815,26.8137389172578,-37.4738412846964));
#57223=CARTESIAN_POINT('Ctrl Pts',(-25.8425080233662,26.746195860494,-37.4679878363966));
#57224=CARTESIAN_POINT('Ctrl Pts',(-25.9367860244216,26.6785759926084,-37.4621277314551));
#57225=CARTESIAN_POINT('Ctrl Pts',(-26.0280033749201,26.6068282703091,-37.4562676265136));
#57226=CARTESIAN_POINT('Ctrl Pts',(-26.115793243649,26.5312741443805,-37.4504075215721));
#57227=CARTESIAN_POINT('Ctrl Pts',(-26.2036422333607,26.455669137476,-37.4445434702166));
#57228=CARTESIAN_POINT('Ctrl Pts',(-26.2880588448778,26.3762529053144,-37.4386794188611));
#57229=CARTESIAN_POINT('Ctrl Pts',(-26.3687134582335,26.2933834081876,-37.4328153675056));
#57230=CARTESIAN_POINT('Ctrl Pts',(-26.4494869403885,26.2103917779649,-37.4269426737091));
#57231=CARTESIAN_POINT('Ctrl Pts',(-26.5264870848545,26.1239370328087,-37.4210699799125));
#57232=CARTESIAN_POINT('Ctrl Pts',(-26.5994247896218,26.0344098418268,-37.415197286116));
#57233=CARTESIAN_POINT('Ctrl Pts',(-26.6193939130889,26.0098987945421,-37.4135894407926));
#57234=CARTESIAN_POINT('Ctrl Pts',(-26.6390587807226,25.9851576081264,-37.4119815954692));
#57235=CARTESIAN_POINT('Ctrl Pts',(-26.6584140418247,25.9601946527716,-37.4103737501458));
#57236=CARTESIAN_POINT('Ctrl Pts',(-26.7291514682649,25.8689628575081,-37.4044975783034));
#57237=CARTESIAN_POINT('Ctrl Pts',(-26.7959908196883,25.7744564661028,-37.3986214064611));
#57238=CARTESIAN_POINT('Ctrl Pts',(-26.8586138433327,25.677042232547,-37.3927452346187));
#57239=CARTESIAN_POINT('Ctrl Pts',(-26.9211569946811,25.5797522456028,-37.3868765575173));
#57240=CARTESIAN_POINT('Ctrl Pts',(-26.9794942885468,25.4795621324493,-37.3810078804158));
#57241=CARTESIAN_POINT('Ctrl Pts',(-27.0333477349422,25.3768714862413,-37.3751392033143));
#57242=CARTESIAN_POINT('Ctrl Pts',(-27.087145447102,25.2742871170695,-37.3692765998489));
#57243=CARTESIAN_POINT('Ctrl Pts',(-27.1364683490371,25.1692077231058,-37.3634139963835));
#57244=CARTESIAN_POINT('Ctrl Pts',(-27.1810821829406,25.0620610657453,-37.3575513929181));
#57245=CARTESIAN_POINT('Ctrl Pts',(-27.2256605731297,24.9549995316571,-37.3516934470314));
#57246=CARTESIAN_POINT('Ctrl Pts',(-27.2655371788725,24.8458743797659,-37.3458355011447));
#57247=CARTESIAN_POINT('Ctrl Pts',(-27.3005243861613,24.735136499681,-37.339977555258));
#57248=CARTESIAN_POINT('Ctrl Pts',(-27.3354938900251,24.6244546526406,-37.3341225734748));
#57249=CARTESIAN_POINT('Ctrl Pts',(-27.3655787921991,24.5121620925942,-37.3282675916916));
#57250=CARTESIAN_POINT('Ctrl Pts',(-27.3906404183595,24.3987275637102,-37.3224126099085));
#57251=CARTESIAN_POINT('Ctrl Pts',(-27.4156946046748,24.28532670923,-37.316559366247));
#57252=CARTESIAN_POINT('Ctrl Pts',(-27.4357283956122,24.1707849630344,-37.3107061225856));
#57253=CARTESIAN_POINT('Ctrl Pts',(-27.4506537679473,24.0555833107248,-37.3048528789242));
#57254=CARTESIAN_POINT('Ctrl Pts',(-27.4655812071526,23.9403657052536,-37.2989988247037));
#57255=CARTESIAN_POINT('Ctrl Pts',(-27.4753987597261,23.8244884195871,-37.2931447704833));
#57256=CARTESIAN_POINT('Ctrl Pts',(-27.480070080354,23.7084392386109,-37.2872907162628));
#57257=CARTESIAN_POINT('Ctrl Pts',(-27.4822318146903,23.6547354749008,-37.2845816515201));
#57258=CARTESIAN_POINT('Ctrl Pts',(-27.4832921953411,23.6009949538121,-37.2818725867774));
#57259=CARTESIAN_POINT('Ctrl Pts',(-27.4832513978708,23.5472661202319,-37.2791635220347));
#57260=CARTESIAN_POINT('',(-27.4892186348263,23.5489291036097,-36.0291635220347));
#57261=CARTESIAN_POINT('Ctrl Pts',(-27.4793303240496,23.5472396509144,-37.2791620358212));
#57262=CARTESIAN_POINT('Ctrl Pts',(-27.4824652871287,23.1002827872345,-37.2566036368044));
#57263=CARTESIAN_POINT('Ctrl Pts',(-27.2053647626636,21.343565728798,-37.1677496006624));
#57264=CARTESIAN_POINT('Ctrl Pts',(-24.614878454963,19.0217514026673,-37.012599927396));
#57265=CARTESIAN_POINT('Ctrl Pts',(-20.3158239957554,20.2067180428611,-36.813713016021));
#57266=CARTESIAN_POINT('Ctrl Pts',(-18.9889351267585,24.4641093933195,-36.6148261046462));
#57267=CARTESIAN_POINT('Ctrl Pts',(-21.8535102169566,27.881743770226,-36.4159391932714));
#57268=CARTESIAN_POINT('Ctrl Pts',(-26.1957055928295,27.3294759798774,-36.2207183324008));
#57269=CARTESIAN_POINT('Ctrl Pts',(-27.4838407068465,24.7818274601648,-36.0917931086553));
#57270=CARTESIAN_POINT('Ctrl Pts',(-27.4892186348263,23.5489291036097,-36.0291635220347));
#57271=CARTESIAN_POINT('',(-27.4833700092727,23.5538806451607,-34.7791635220347));
#57272=CARTESIAN_POINT('Ctrl Pts',(-27.4892186348263,23.5489291036097,-36.0291635220347));
#57273=CARTESIAN_POINT('Ctrl Pts',(-27.489533434215,23.4767608539724,-36.0254974715303));
#57274=CARTESIAN_POINT('Ctrl Pts',(-27.4549757162681,22.099833590961,-35.9555357839008));
#57275=CARTESIAN_POINT('Ctrl Pts',(-25.8447397533594,19.503515670751,-35.8192784591468));
#57276=CARTESIAN_POINT('Ctrl Pts',(-21.3859325269578,19.4324291079409,-35.6203915477717));
#57277=CARTESIAN_POINT('Ctrl Pts',(-18.9159518808349,23.1452731377106,-35.4215046363969));
#57278=CARTESIAN_POINT('Ctrl Pts',(-20.7045006089515,27.2302588939586,-35.222617725022));
#57279=CARTESIAN_POINT('Ctrl Pts',(-25.1080540740967,27.9336308163746,-35.023730813647));
#57280=CARTESIAN_POINT('Ctrl Pts',(-27.316972897996,25.462713316296,-34.8759127459847));
#57281=CARTESIAN_POINT('Ctrl Pts',(-27.4861582946516,23.8547890233352,-34.7943903154472));
#57282=CARTESIAN_POINT('Ctrl Pts',(-27.4833700092727,23.5538806451607,-34.7791635220347));
#57283=CARTESIAN_POINT('',(-27.4767519051405,23.5499334425378,-33.5291635220347));
#57284=CARTESIAN_POINT('Ctrl Pts',(-27.4833700092727,23.5538806451607,-34.7791635220347));
#57285=CARTESIAN_POINT('Ctrl Pts',(-27.4740184336399,22.5446699387121,-34.7280946783222));
#57286=CARTESIAN_POINT('Ctrl Pts',(-26.5635452019007,20.2103566681747,-34.6107301974847));
#57287=CARTESIAN_POINT('Ctrl Pts',(-22.6305263658179,18.9901149666739,-34.4270700795225));
#57288=CARTESIAN_POINT('Ctrl Pts',(-19.2165813045135,21.8590859145908,-34.2281831681474));
#57289=CARTESIAN_POINT('Ctrl Pts',(-19.7849126662585,26.2820955963449,-34.0292962567727));
#57290=CARTESIAN_POINT('Ctrl Pts',(-23.8132721161679,28.1947731237778,-33.8304093453977));
#57291=CARTESIAN_POINT('Ctrl Pts',(-26.9873304880107,26.2205621386255,-33.6636984338185));
#57292=CARTESIAN_POINT('Ctrl Pts',(-27.4762637887713,24.2270688085383,-33.5632831593641));
#57293=CARTESIAN_POINT('Ctrl Pts',(-27.4767519051405,23.5499334425378,-33.5291635220347));
#57294=CARTESIAN_POINT('',(-27.4845450668246,23.5467337760579,-32.2791635220347));
#57295=CARTESIAN_POINT('Ctrl Pts',(-27.4767519051405,23.5499334425378,-33.5291635220347));
#57296=CARTESIAN_POINT('Ctrl Pts',(-27.4772122157835,22.9113713386183,-33.4969875222391));
#57297=CARTESIAN_POINT('Ctrl Pts',(-27.0277930863398,20.9577225774089,-33.3985158853185));
#57298=CARTESIAN_POINT('Ctrl Pts',(-23.9492676055535,18.9154345414229,-33.2337486112731));
#57299=CARTESIAN_POINT('Ctrl Pts',(-19.8665869552278,20.7092388476606,-33.0348616998981));
#57300=CARTESIAN_POINT('Ctrl Pts',(-19.1688826463395,25.1136938512856,-32.8359747885233));
#57301=CARTESIAN_POINT('Ctrl Pts',(-22.4972857831852,28.0814788401733,-32.6370878771483));
#57302=CARTESIAN_POINT('Ctrl Pts',(-26.5063577130066,26.9653307208194,-32.4514841216523));
#57303=CARTESIAN_POINT('Ctrl Pts',(-27.4748464854124,24.5935520426802,-32.332176003281));
#57304=CARTESIAN_POINT('Ctrl Pts',(-27.4845450668246,23.5467337760579,-32.2791635220347));
#57305=CARTESIAN_POINT('',(-27.4885670794543,23.5522069440821,-31.0291635220347));
#57306=CARTESIAN_POINT('Ctrl Pts',(-27.4845450668246,23.5467337760579,-32.2791635220347));
#57307=CARTESIAN_POINT('Ctrl Pts',(-27.4869752071552,23.2844361079365,-32.265880366156));
#57308=CARTESIAN_POINT('Ctrl Pts',(-27.3433199675825,21.7156705685443,-32.1863015731523));
#57309=CARTESIAN_POINT('Ctrl Pts',(-25.2358406503036,19.2144084931583,-32.0404271430236));
#57310=CARTESIAN_POINT('Ctrl Pts',(-20.8135660294717,19.7884314539895,-31.8415402316489));
#57311=CARTESIAN_POINT('Ctrl Pts',(-18.9060742714317,23.8192490354008,-31.642653320274));
#57312=CARTESIAN_POINT('Ctrl Pts',(-21.2661885731902,27.6028816370503,-31.443766408899));
#57313=CARTESIAN_POINT('Ctrl Pts',(-25.7251639961269,27.6624916971592,-31.2448794975241));
#57314=CARTESIAN_POINT('Ctrl Pts',(-27.4348385173242,25.0781310411118,-31.106678535236));
#57315=CARTESIAN_POINT('Ctrl Pts',(-27.4892390080544,23.6626852313028,-31.0347732100729));
#57316=CARTESIAN_POINT('Ctrl Pts',(-27.4885670794543,23.5522069440821,-31.0291635220347));
#57317=CARTESIAN_POINT('',(-27.4784969839717,23.5528208098879,-29.7791635220347));
#57318=CARTESIAN_POINT('Ctrl Pts',(-27.4885670794543,23.5522069440821,-31.0291635220347));
#57319=CARTESIAN_POINT('Ctrl Pts',(-27.4812981146679,22.3570460602959,-30.9684775729479));
#57320=CARTESIAN_POINT('Ctrl Pts',(-26.2622685644213,19.8434146916342,-30.8414959867364));
#57321=CARTESIAN_POINT('Ctrl Pts',(-21.9811740242355,19.1708983019553,-30.6482187633994));
#57322=CARTESIAN_POINT('Ctrl Pts',(-19.0176748890843,22.5031179912306,-30.4493318520245));
#57323=CARTESIAN_POINT('Ctrl Pts',(-20.2192303082857,26.7975655408241,-30.2504449406496));
#57324=CARTESIAN_POINT('Ctrl Pts',(-24.4817127266861,28.1080077617663,-30.0515580292749));
#57325=CARTESIAN_POINT('Ctrl Pts',(-27.1724268576346,25.8349750791294,-29.8944642230698));
#57326=CARTESIAN_POINT('Ctrl Pts',(-27.481392228598,24.0385560742375,-29.8036660539898));
#57327=CARTESIAN_POINT('Ctrl Pts',(-27.4784969839717,23.5528208098879,-29.7791635220347));
#57328=CARTESIAN_POINT('',(-27.4826813963389,23.5473322497447,-28.5291634804562));
#57329=CARTESIAN_POINT('Ctrl Pts',(-27.4784969839717,23.5528208098879,-29.7791635220347));
#57330=CARTESIAN_POINT('Ctrl Pts',(-27.4735586672547,22.7243192891093,-29.7373704168648));
#57331=CARTESIAN_POINT('Ctrl Pts',(-26.8116566502793,20.5743666249437,-29.62928167457));
#57332=CARTESIAN_POINT('Ctrl Pts',(-23.2752795542552,18.9064242947988,-29.4548972951501));
#57333=CARTESIAN_POINT('Ctrl Pts',(-19.49468736946,21.2714058832831,-29.2560103837753));
#57334=CARTESIAN_POINT('Ctrl Pts',(-19.440815713535,25.7304543273257,-29.0571234724003));
#57335=CARTESIAN_POINT('Ctrl Pts',(-23.1631680707165,28.1860821718098,-28.8582365610254));
#57336=CARTESIAN_POINT('Ctrl Pts',(-26.771662874525,26.5895273166329,-28.6822499109035));
#57337=CARTESIAN_POINT('Ctrl Pts',(-27.4732871731943,24.4072281778359,-28.5725588979067));
#57338=CARTESIAN_POINT('Ctrl Pts',(-27.4791742225268,23.5473356782317,-28.5291635220347));
#57339=CARTESIAN_POINT('',(-27.4847176457149,23.5488150353494,-27.2791635220347));
#57340=CARTESIAN_POINT('Ctrl Pts',(-27.4832514471146,23.5473316924836,-28.5291634736981));
#57341=CARTESIAN_POINT('Ctrl Pts',(-27.4831520660432,23.4135120543238,-28.5224170883845));
#57342=CARTESIAN_POINT('Ctrl Pts',(-27.4762189501434,23.2799706350553,-28.515670703071));
#57343=CARTESIAN_POINT('Ctrl Pts',(-27.4625607997496,23.1473468160422,-28.5089243177574));
#57344=CARTESIAN_POINT('Ctrl Pts',(-27.4488274434656,23.0139927303323,-28.5021407848141));
#57345=CARTESIAN_POINT('Ctrl Pts',(-27.4282949044146,22.8815665128418,-28.4953572518708));
#57346=CARTESIAN_POINT('Ctrl Pts',(-27.4011229596204,22.7506989391669,-28.4885737189276));
#57347=CARTESIAN_POINT('Ctrl Pts',(-27.3737751256306,22.6189842346574,-28.4817462748781));
#57348=CARTESIAN_POINT('Ctrl Pts',(-27.3397017424326,22.4888485496326,-28.4749188308287));
#57349=CARTESIAN_POINT('Ctrl Pts',(-27.299113931195,22.3609135525412,-28.4680913867792));
#57350=CARTESIAN_POINT('Ctrl Pts',(-27.2839969931815,22.3132641385466,-28.4655485039447));
#57351=CARTESIAN_POINT('Ctrl Pts',(-27.2679768501773,22.2659197797332,-28.4630056211102));
#57352=CARTESIAN_POINT('Ctrl Pts',(-27.2510660667031,22.2189117867702,-28.4604627382757));
#57353=CARTESIAN_POINT('Ctrl Pts',(-27.2120138771227,22.1103559025446,-28.454590441307));
#57354=CARTESIAN_POINT('Ctrl Pts',(-27.1681158137966,22.0033378902036,-28.4487181443383));
#57355=CARTESIAN_POINT('Ctrl Pts',(-27.1195122154757,21.8983220520033,-28.4428458473695));
#57356=CARTESIAN_POINT('Ctrl Pts',(-27.0709716035582,21.793442305989,-28.4369811604313));
#57357=CARTESIAN_POINT('Ctrl Pts',(-27.0177377554039,21.6905599459593,-28.4311164734931));
#57358=CARTESIAN_POINT('Ctrl Pts',(-26.9600002446536,21.590122552849,-28.4252517865549));
#57359=CARTESIAN_POINT('Ctrl Pts',(-26.9023221133187,21.4897884533098,-28.41939313108));
#57360=CARTESIAN_POINT('Ctrl Pts',(-26.8401497369302,21.3918946754604,-28.4135344756052));
#57361=CARTESIAN_POINT('Ctrl Pts',(-26.7737197968873,21.2968666814172,-28.4076758201303));
#57362=CARTESIAN_POINT('Ctrl Pts',(-26.7046950448759,21.1981268102276,-28.4015883204124));
#57363=CARTESIAN_POINT('Ctrl Pts',(-26.6310735312265,21.1024815795914,-28.3955008206945));
#57364=CARTESIAN_POINT('Ctrl Pts',(-26.5531722413835,21.0103780826005,-28.3894133209766));
#57365=CARTESIAN_POINT('Ctrl Pts',(-26.4782862867854,20.9218396475129,-28.3835614508932));
#57366=CARTESIAN_POINT('Ctrl Pts',(-26.3994460029958,20.8365742086214,-28.3777095808098));
#57367=CARTESIAN_POINT('Ctrl Pts',(-26.3169752153742,20.7549467180826,-28.3718577107264));
#57368=CARTESIAN_POINT('Ctrl Pts',(-26.2345169846798,20.6733316560714,-28.3660067316434));
#57369=CARTESIAN_POINT('Ctrl Pts',(-26.1484296429749,20.595353731781,-28.3601557525604));
#57370=CARTESIAN_POINT('Ctrl Pts',(-26.0590742194072,20.5213413842254,-28.3543047734774));
#57371=CARTESIAN_POINT('Ctrl Pts',(-25.9697107619269,20.4473223822474,-28.3484532683351));
#57372=CARTESIAN_POINT('Ctrl Pts',(-25.8770789568492,20.3772699294884,-28.3426017631928));
#57373=CARTESIAN_POINT('Ctrl Pts',(-25.7815727191508,20.3114720172029,-28.3367502580505));
#57374=CARTESIAN_POINT('Ctrl Pts',(-25.6860347659098,20.245652254863,-28.3308968097507));
#57375=CARTESIAN_POINT('Ctrl Pts',(-25.5876208222482,20.1840900767421,-28.3250433614509));
#57376=CARTESIAN_POINT('Ctrl Pts',(-25.4867529475112,20.1270296146845,-28.3191899131511));
#57377=CARTESIAN_POINT('Ctrl Pts',(-25.3857703640979,20.0699042624912,-28.3133298082095));
#57378=CARTESIAN_POINT('Ctrl Pts',(-25.2823286395667,20.0172910482452,-28.307469703268));
#57379=CARTESIAN_POINT('Ctrl Pts',(-25.1768736337033,19.969387721275,-28.3016095983264));
#57380=CARTESIAN_POINT('Ctrl Pts',(-25.0713476104936,19.9214521344121,-28.2957455469709));
#57381=CARTESIAN_POINT('Ctrl Pts',(-24.9638059888764,19.8782329043096,-28.2898814956155));
#57382=CARTESIAN_POINT('Ctrl Pts',(-24.8547121167039,19.8398786703325,-28.28401744426));
#57383=CARTESIAN_POINT('Ctrl Pts',(-24.7454574619413,19.8014679098708,-28.2781447504634));
#57384=CARTESIAN_POINT('Ctrl Pts',(-24.6346463849799,19.7679365748156,-28.2722720566669));
#57385=CARTESIAN_POINT('Ctrl Pts',(-24.5227548832301,19.7393827915618,-28.2663993628703));
#57386=CARTESIAN_POINT('Ctrl Pts',(-24.4921208617703,19.7315652433541,-28.2647915175471));
#57387=CARTESIAN_POINT('Ctrl Pts',(-24.4614058959691,19.7241205002501,-28.2631836722239));
#57388=CARTESIAN_POINT('Ctrl Pts',(-24.4306198297197,19.7170498993556,-28.2615758269007));
#57389=CARTESIAN_POINT('Ctrl Pts',(-24.3181805789353,19.6912261042424,-28.255703529932));
#57390=CARTESIAN_POINT('Ctrl Pts',(-24.2044157653797,19.6703105089654,-28.2498312329633));
#57391=CARTESIAN_POINT('Ctrl Pts',(-24.0897918733749,19.6544360192313,-28.2439589359946));
#57392=CARTESIAN_POINT('Ctrl Pts',(-23.975316524831,19.6385821015751,-28.2380942490564));
#57393=CARTESIAN_POINT('Ctrl Pts',(-23.8599847174821,19.6277563541091,-28.2322295621182));
#57394=CARTESIAN_POINT('Ctrl Pts',(-23.7442754812678,19.6220412218181,-28.22636487518));
#57395=CARTESIAN_POINT('Ctrl Pts',(-23.6286852447595,19.6163319671828,-28.2205062197052));
#57396=CARTESIAN_POINT('Ctrl Pts',(-23.5127187618572,19.6157228936424,-28.2146475642303));
#57397=CARTESIAN_POINT('Ctrl Pts',(-23.3968619173076,19.6202448574755,-28.2087889087555));
#57398=CARTESIAN_POINT('Ctrl Pts',(-23.2764796023646,19.6249434531987,-28.2027014090376));
#57399=CARTESIAN_POINT('Ctrl Pts',(-23.156216115906,19.6351821660239,-28.1966139093197));
#57400=CARTESIAN_POINT('Ctrl Pts',(-23.0366189489219,19.6509359835478,-28.1905264096018));
#57401=CARTESIAN_POINT('Ctrl Pts',(-22.9216510448618,19.6660800160307,-28.1846745395184));
#57402=CARTESIAN_POINT('Ctrl Pts',(-22.8072992848527,19.6863200852052,-28.178822669435));
#57403=CARTESIAN_POINT('Ctrl Pts',(-22.6940457506019,19.7115810234753,-28.1729707993516));
#57404=CARTESIAN_POINT('Ctrl Pts',(-22.5808094602314,19.7368381155378,-28.1671198202686));
#57405=CARTESIAN_POINT('Ctrl Pts',(-22.4686714665002,19.7671144667109,-28.1612688411857));
#57406=CARTESIAN_POINT('Ctrl Pts',(-22.3581032422207,19.8022838723258,-28.1554178621027));
#57407=CARTESIAN_POINT('Ctrl Pts',(-22.2475250767937,19.8374564400087,-28.1495663569604));
#57408=CARTESIAN_POINT('Ctrl Pts',(-22.1385173553449,19.8775228113692,-28.1437148518181));
#57409=CARTESIAN_POINT('Ctrl Pts',(-22.0315352974928,19.9223072506102,-28.1378633466758));
#57410=CARTESIAN_POINT('Ctrl Pts',(-21.9245177132281,19.9671065617886,-28.132009898376));
#57411=CARTESIAN_POINT('Ctrl Pts',(-21.8195275112575,20.016626896724,-28.1261564500762));
#57412=CARTESIAN_POINT('Ctrl Pts',(-21.7169982247661,20.0706451334193,-28.1203030017764));
#57413=CARTESIAN_POINT('Ctrl Pts',(-21.6143523402122,20.1247248005795,-28.1144428968349));
#57414=CARTESIAN_POINT('Ctrl Pts',(-21.5141733229946,20.1833123862658,-28.1085827918934));
#57415=CARTESIAN_POINT('Ctrl Pts',(-21.4168685490566,20.246139673055,-28.1027226869518));
#57416=CARTESIAN_POINT('Ctrl Pts',(-21.3194982464434,20.3090092700896,-28.0968586355964));
#57417=CARTESIAN_POINT('Ctrl Pts',(-21.2250063775183,20.3761240146521,-28.0909945842409));
#57418=CARTESIAN_POINT('Ctrl Pts',(-21.1337684542299,20.4471744302985,-28.0851305328855));
#57419=CARTESIAN_POINT('Ctrl Pts',(-21.0423960644554,20.5183295600745,-28.0792578390889));
#57420=CARTESIAN_POINT('Ctrl Pts',(-20.9542875049638,20.5934316702461,-28.0733851452923));
#57421=CARTESIAN_POINT('Ctrl Pts',(-20.8697826279166,20.6721333376818,-28.0675124514957));
#57422=CARTESIAN_POINT('Ctrl Pts',(-20.8466466061759,20.6936805377068,-28.0659046061725));
#57423=CARTESIAN_POINT('Ctrl Pts',(-20.823780477776,20.7154973545272,-28.0642967608492));
#57424=CARTESIAN_POINT('Ctrl Pts',(-20.801190688688,20.7375762290729,-28.0626889155259));
#57425=CARTESIAN_POINT('Ctrl Pts',(-20.7186865148945,20.8182144012839,-28.0568166185572));
#57426=CARTESIAN_POINT('Ctrl Pts',(-20.6395951691016,20.9026208817799,-28.0509443215885));
#57427=CARTESIAN_POINT('Ctrl Pts',(-20.5642806216622,20.9904750506424,-28.0450720246198));
#57428=CARTESIAN_POINT('Ctrl Pts',(-20.4890636758949,21.0782153674793,-28.0392073376817));
#57429=CARTESIAN_POINT('Ctrl Pts',(-20.4176140617805,21.1693941766258,-28.0333426507435));
#57430=CARTESIAN_POINT('Ctrl Pts',(-20.3502600776578,21.2636530271656,-28.0274779638053));
#57431=CARTESIAN_POINT('Ctrl Pts',(-20.2829753628914,21.3578149383784,-28.0216193083305));
#57432=CARTESIAN_POINT('Ctrl Pts',(-20.2197781389261,21.4550502560889,-28.0157606528557));
#57433=CARTESIAN_POINT('Ctrl Pts',(-20.1609570069702,21.5549668764342,-28.0099019973809));
#57434=CARTESIAN_POINT('Ctrl Pts',(-20.0998382697911,21.658786327976,-28.003814497663));
#57435=CARTESIAN_POINT('Ctrl Pts',(-20.0434447579164,21.765500475276,-27.997726997945));
#57436=CARTESIAN_POINT('Ctrl Pts',(-19.9920513700819,21.874635184714,-27.9916394982271));
#57437=CARTESIAN_POINT('Ctrl Pts',(-19.9426472727203,21.9795456029174,-27.9857876281438));
#57438=CARTESIAN_POINT('Ctrl Pts',(-19.8978636085097,22.0866922726609,-27.9799357580604));
#57439=CARTESIAN_POINT('Ctrl Pts',(-19.8578977232899,22.1956289792436,-27.974083887977));
#57440=CARTESIAN_POINT('Ctrl Pts',(-19.8179379232396,22.3045490992222,-27.968232908894));
#57441=CARTESIAN_POINT('Ctrl Pts',(-19.7827945859869,22.4152583261415,-27.9623819298111));
#57442=CARTESIAN_POINT('Ctrl Pts',(-19.7526163844688,22.5272917830402,-27.9565309507281));
#57443=CARTESIAN_POINT('Ctrl Pts',(-19.7224354696399,22.6393353128249,-27.9506794455858));
#57444=CARTESIAN_POINT('Ctrl Pts',(-19.6972206855005,22.7527029100921,-27.9448279404435));
#57445=CARTESIAN_POINT('Ctrl Pts',(-19.6770702480778,22.8669165982909,-27.9389764353013));
#57446=CARTESIAN_POINT('Ctrl Pts',(-19.6569131191335,22.9811682143692,-27.9331229870015));
#57447=CARTESIAN_POINT('Ctrl Pts',(-19.6418237527632,23.0962660731868,-27.9272695387017));
#57448=CARTESIAN_POINT('Ctrl Pts',(-19.6318487757525,23.2117248291026,-27.921416090402));
#57449=CARTESIAN_POINT('Ctrl Pts',(-19.6218624550269,23.3273148866953,-27.9155559854605));
#57450=CARTESIAN_POINT('Ctrl Pts',(-19.6170021681654,23.4432662484759,-27.9096958805189));
#57451=CARTESIAN_POINT('Ctrl Pts',(-19.6172624633169,23.5590911993404,-27.9038357755774));
#57452=CARTESIAN_POINT('Ctrl Pts',(-19.617522933761,23.6749941510601,-27.897971724222));
#57453=CARTESIAN_POINT('Ctrl Pts',(-19.6229108334802,23.7907701104263,-27.8921076728665));
#57454=CARTESIAN_POINT('Ctrl Pts',(-19.6333687748771,23.9059358677986,-27.8862436215111));
#57455=CARTESIAN_POINT('Ctrl Pts',(-19.643842129192,24.021271356508,-27.8803709277145));
#57456=CARTESIAN_POINT('Ctrl Pts',(-19.6594003829685,24.1359944402673,-27.874498233918));
#57457=CARTESIAN_POINT('Ctrl Pts',(-19.6799349477978,24.2496313988199,-27.8686255401214));
#57458=CARTESIAN_POINT('Ctrl Pts',(-19.6855569681471,24.28074329716,-27.867017694798));
#57459=CARTESIAN_POINT('Ctrl Pts',(-19.6915517104226,24.3117738690118,-27.8654098494745));
#57460=CARTESIAN_POINT('Ctrl Pts',(-19.6979162993722,24.3427136052739,-27.8638020041511));
#57461=CARTESIAN_POINT('Ctrl Pts',(-19.7211615430849,24.455714101537,-27.8579297071824));
#57462=CARTESIAN_POINT('Ctrl Pts',(-19.7494219059978,24.5678802587197,-27.8520574102136));
#57463=CARTESIAN_POINT('Ctrl Pts',(-19.7826243865996,24.6787325537996,-27.8461851132449));
#57464=CARTESIAN_POINT('Ctrl Pts',(-19.8157838394234,24.7894411931088,-27.8403204263067));
#57465=CARTESIAN_POINT('Ctrl Pts',(-19.853872555986,24.8988389639505,-27.8344557393685));
#57466=CARTESIAN_POINT('Ctrl Pts',(-19.8967664246872,25.006455905508,-27.8285910524303));
#57467=CARTESIAN_POINT('Ctrl Pts',(-19.9396161797296,25.113962169778,-27.8227323969555));
#57468=CARTESIAN_POINT('Ctrl Pts',(-19.9872611052841,25.2196908659592,-27.8168737414807));
#57469=CARTESIAN_POINT('Ctrl Pts',(-20.0395273189796,25.3231872402522,-27.8110150860059));
#57470=CARTESIAN_POINT('Ctrl Pts',(-20.0938350970176,25.4307262740836,-27.804927586288));
#57471=CARTESIAN_POINT('Ctrl Pts',(-20.1531324157586,25.5358546023575,-27.7988400865701));
#57472=CARTESIAN_POINT('Ctrl Pts',(-20.2171689730529,25.6380846588336,-27.7927525868522));
#57473=CARTESIAN_POINT('Ctrl Pts',(-20.2787268590882,25.7363576833655,-27.7869007167688));
#57474=CARTESIAN_POINT('Ctrl Pts',(-20.3446636810568,25.8319522487235,-27.7810488466854));
#57475=CARTESIAN_POINT('Ctrl Pts',(-20.4147107048366,25.9244611265793,-27.775196976602));
#57476=CARTESIAN_POINT('Ctrl Pts',(-20.4847470633201,26.0169559191173,-27.769345997519));
#57477=CARTESIAN_POINT('Ctrl Pts',(-20.5588921298173,26.1063656288389,-27.763495018436));
#57478=CARTESIAN_POINT('Ctrl Pts',(-20.6368351595661,26.1923138890026,-27.7576440393531));
#57479=CARTESIAN_POINT('Ctrl Pts',(-20.7147851971434,26.278269876742,-27.7517925342108));
#57480=CARTESIAN_POINT('Ctrl Pts',(-20.7965335990762,26.360763490015,-27.7459410290685));
#57481=CARTESIAN_POINT('Ctrl Pts',(-20.8817313255989,26.4394537314412,-27.7400895239262));
#57482=CARTESIAN_POINT('Ctrl Pts',(-20.9669573444319,26.5181701041836,-27.7342360756264));
#57483=CARTESIAN_POINT('Ctrl Pts',(-21.0556346619889,26.5930803133196,-27.7283826273266));
#57484=CARTESIAN_POINT('Ctrl Pts',(-21.1473801525931,26.663882781058,-27.7225291790269));
#57485=CARTESIAN_POINT('Ctrl Pts',(-21.2392299777422,26.7347657665766,-27.7166690740853));
#57486=CARTESIAN_POINT('Ctrl Pts',(-21.3341546127783,26.8015314340299,-27.7108089691438));
#57487=CARTESIAN_POINT('Ctrl Pts',(-21.4317407878446,26.863920739462,-27.7049488642023));
#57488=CARTESIAN_POINT('Ctrl Pts',(-21.5293926810921,26.9263520601866,-27.6990848128468));
#57489=CARTESIAN_POINT('Ctrl Pts',(-21.6297093264324,26.984400943882,-27.6932207614914));
#57490=CARTESIAN_POINT('Ctrl Pts',(-21.7322531710581,27.0378544764016,-27.6873567101359));
#57491=CARTESIAN_POINT('Ctrl Pts',(-21.8349481448411,27.0913867887578,-27.6814840163394));
#57492=CARTESIAN_POINT('Ctrl Pts',(-21.9398764957877,27.1403100590439,-27.6756113225428));
#57493=CARTESIAN_POINT('Ctrl Pts',(-22.0465809784596,27.1844595786293,-27.6697386287463));
#57494=CARTESIAN_POINT('Ctrl Pts',(-22.0757948808678,27.1965469785609,-27.6681307834229));
#57495=CARTESIAN_POINT('Ctrl Pts',(-22.1051418339389,27.2082768408679,-27.6665229380995));
#57496=CARTESIAN_POINT('Ctrl Pts',(-22.1346122833106,27.2196464444755,-27.6649150927761));
#57497=CARTESIAN_POINT('Ctrl Pts',(-22.2422465364298,27.2611713895868,-27.6590427958074));
#57498=CARTESIAN_POINT('Ctrl Pts',(-22.3518897306156,27.2980260351271,-27.6531704988387));
#57499=CARTESIAN_POINT('Ctrl Pts',(-22.4630989746921,27.3300125959704,-27.64729820187));
#57500=CARTESIAN_POINT('Ctrl Pts',(-22.5741641004203,27.3619577047713,-27.6414335149318));
#57501=CARTESIAN_POINT('Ctrl Pts',(-22.68679084653,27.3890471613059,-27.6355688279936));
#57502=CARTESIAN_POINT('Ctrl Pts',(-22.8005167395195,27.4111313490015,-27.6297041410553));
#57503=CARTESIAN_POINT('Ctrl Pts',(-22.9141256725473,27.4331928244925,-27.6238454855805));
#57504=CARTESIAN_POINT('Ctrl Pts',(-23.0288311006609,27.4502591916687,-27.6179868301057));
#57505=CARTESIAN_POINT('Ctrl Pts',(-23.1441564410661,27.4622309269792,-27.6121281746308));
#57506=CARTESIAN_POINT('Ctrl Pts',(-23.2639864908444,27.4746702888155,-27.6060406749129));
#57507=CARTESIAN_POINT('Ctrl Pts',(-23.3844854318614,27.4816087777917,-27.599953175195));
#57508=CARTESIAN_POINT('Ctrl Pts',(-23.5051077675357,27.4829934270837,-27.5938656754771));
#57509=CARTESIAN_POINT('Ctrl Pts',(-23.6210611589498,27.4843244805774,-27.5880138053937));
#57510=CARTESIAN_POINT('Ctrl Pts',(-23.7371281182293,27.4805236410682,-27.5821619353103));
#57511=CARTESIAN_POINT('Ctrl Pts',(-23.8528207751636,27.4715968749066,-27.5763100652269));
#57512=CARTESIAN_POINT('Ctrl Pts',(-23.9684958168387,27.4626714679263,-27.5704590861439));
#57513=CARTESIAN_POINT('Ctrl Pts',(-24.0837962574401,27.448621717909,-27.5646081070609));
#57514=CARTESIAN_POINT('Ctrl Pts',(-24.198237482596,27.4295056174576,-27.558757127978));
#57515=CARTESIAN_POINT('Ctrl Pts',(-24.3126889971193,27.4103877982848,-27.5529056228357));
#57516=CARTESIAN_POINT('Ctrl Pts',(-24.4262807348698,27.3862027912702,-27.5470541176933));
#57517=CARTESIAN_POINT('Ctrl Pts',(-24.5385371382397,27.3570599258849,-27.541202612551));
#57518=CARTESIAN_POINT('Ctrl Pts',(-24.6508308195173,27.3279073827885,-27.5353491642513));
#57519=CARTESIAN_POINT('Ctrl Pts',(-24.7617878847632,27.2937938113849,-27.5294957159515));
#57520=CARTESIAN_POINT('Ctrl Pts',(-24.8709475158518,27.2548785261531,-27.5236422676517));
#57521=CARTESIAN_POINT('Ctrl Pts',(-24.9802312851447,27.2159189857918,-27.5177821627102));
#57522=CARTESIAN_POINT('Ctrl Pts',(-25.087713150762,27.1721469713227,-27.5119220577686));
#57523=CARTESIAN_POINT('Ctrl Pts',(-25.1929517848003,27.1237701493707,-27.5060619528271));
#57524=CARTESIAN_POINT('Ctrl Pts',(-25.298261290472,27.075360748657,-27.5001979014716));
#57525=CARTESIAN_POINT('Ctrl Pts',(-25.4013241898144,27.0223405542987,-27.4943338501162));
#57526=CARTESIAN_POINT('Ctrl Pts',(-25.5017248387421,26.9649625976918,-27.4884697987607));
#57527=CARTESIAN_POINT('Ctrl Pts',(-25.6022734581846,26.9075000774305,-27.4825971049641));
#57528=CARTESIAN_POINT('Ctrl Pts',(-25.7001516482383,26.8456671968592,-27.4767244111675));
#57529=CARTESIAN_POINT('Ctrl Pts',(-25.7949736762255,26.7797596122398,-27.470851717371));
#57530=CARTESIAN_POINT('Ctrl Pts',(-25.820934361308,26.7617152180713,-27.4692438720477));
#57531=CARTESIAN_POINT('Ctrl Pts',(-25.846666163512,26.7433656219047,-27.4676360267245));
#57532=CARTESIAN_POINT('Ctrl Pts',(-25.8721616290135,26.7247173911289,-27.4660281814012));
#57533=CARTESIAN_POINT('Ctrl Pts',(-25.9644504744281,26.6572142624953,-27.4602080802354));
#57534=CARTESIAN_POINT('Ctrl Pts',(-26.0539612220893,26.5855601120598,-27.4543879790697));
#57535=CARTESIAN_POINT('Ctrl Pts',(-26.1402920289457,26.5100134008654,-27.4485678779039));
#57536=CARTESIAN_POINT('Ctrl Pts',(-26.2265105992982,26.4345649060442,-27.4427553433048));
#57537=CARTESIAN_POINT('Ctrl Pts',(-26.3095571329673,26.3552341851834,-27.4369428087057));
#57538=CARTESIAN_POINT('Ctrl Pts',(-26.3890593711334,26.2723224662023,-27.4311302741066));
#57539=CARTESIAN_POINT('Ctrl Pts',(-26.4684804720688,26.18949536405,-27.425323671579));
#57540=CARTESIAN_POINT('Ctrl Pts',(-26.5443641797559,26.1030948327763,-27.4195170690514));
#57541=CARTESIAN_POINT('Ctrl Pts',(-26.6163725091683,26.0134612690394,-27.4137104665238));
#57542=CARTESIAN_POINT('Ctrl Pts',(-26.6883287911869,25.9238924921604,-27.4079080609903));
#57543=CARTESIAN_POINT('Ctrl Pts',(-26.7564150022,25.8310956573359,-27.4021056554567));
#57544=CARTESIAN_POINT('Ctrl Pts',(-26.8203316570448,25.7354462333935,-27.3963032499232));
#57545=CARTESIAN_POINT('Ctrl Pts',(-26.8842242657599,25.6398327937881,-27.3905030273167));
#57546=CARTESIAN_POINT('Ctrl Pts',(-26.9439502017762,25.5413692477434,-27.3847028047102));
#57547=CARTESIAN_POINT('Ctrl Pts',(-26.9992521721443,25.4404616418657,-27.3789025821037));
#57548=CARTESIAN_POINT('Ctrl Pts',(-27.0545473189922,25.3395664866308,-27.3731030751667));
#57549=CARTESIAN_POINT('Ctrl Pts',(-27.1054193830347,25.2362282407594,-27.3673035682298));
#57550=CARTESIAN_POINT('Ctrl Pts',(-27.1516564893883,25.1308785258831,-27.3615040612928));
#57551=CARTESIAN_POINT('Ctrl Pts',(-27.1978995808798,25.0255151740681,-27.3557038036417));
#57552=CARTESIAN_POINT('Ctrl Pts',(-27.2395063536526,24.9181402220512,-27.3499035459907));
#57553=CARTESIAN_POINT('Ctrl Pts',(-27.2763129679182,24.8092055195402,-27.3441032883396));
#57554=CARTESIAN_POINT('Ctrl Pts',(-27.313155386537,24.7001648486686,-27.3382973883745));
#57555=CARTESIAN_POINT('Ctrl Pts',(-27.345188187438,24.5895617975059,-27.3324914884095));
#57556=CARTESIAN_POINT('Ctrl Pts',(-27.3722973508228,24.4778636574209,-27.3266855884444));
#57557=CARTESIAN_POINT('Ctrl Pts',(-27.3994204194904,24.3661082232691,-27.3208767104206));
#57558=CARTESIAN_POINT('Ctrl Pts',(-27.421614740824,24.253256995109,-27.3150678323969));
#57559=CARTESIAN_POINT('Ctrl Pts',(-27.4388177417771,24.1397859123718,-27.3092589543731));
#57560=CARTESIAN_POINT('Ctrl Pts',(-27.4560471045766,24.0261409467597,-27.3034411748355));
#57561=CARTESIAN_POINT('Ctrl Pts',(-27.4682698270097,23.9118746484371,-27.2976233952979));
#57562=CARTESIAN_POINT('Ctrl Pts',(-27.4754753431419,23.7974667717586,-27.2918056157603));
#57563=CARTESIAN_POINT('Ctrl Pts',(-27.4806945629316,23.7145969477095,-27.2875915845184));
#57564=CARTESIAN_POINT('Ctrl Pts',(-27.4832825346391,23.6316528966433,-27.2833775532766));
#57565=CARTESIAN_POINT('Ctrl Pts',(-27.4832522691901,23.5488155707394,-27.2791635220347));
#57566=CARTESIAN_POINT('',(-27.4832508680474,23.5538700228986,-26.0291635220347));
#57567=CARTESIAN_POINT('Ctrl Pts',(-27.4891202243453,23.5488134268231,-27.2791635220347));
#57568=CARTESIAN_POINT('Ctrl Pts',(-27.4894904774531,23.4699199363944,-27.2751561046986));
#57569=CARTESIAN_POINT('Ctrl Pts',(-27.487326383654,23.3910471511404,-27.2711486873625));
#57570=CARTESIAN_POINT('Ctrl Pts',(-27.4037747347876,22.0101217003781,-27.2008456329014));
#57571=CARTESIAN_POINT('Ctrl Pts',(-25.8238780958542,19.4917580292825,-27.0682543586514));
#57572=CARTESIAN_POINT('Ctrl Pts',(-21.364764015651,19.4436248667672,-26.8693674472766));
#57573=CARTESIAN_POINT('Ctrl Pts',(-18.9139285828196,23.1691343437126,-26.6704805359016));
#57574=CARTESIAN_POINT('Ctrl Pts',(-20.7234817635613,27.2448591219192,-26.4715936245267));
#57575=CARTESIAN_POINT('Ctrl Pts',(-25.1305976095771,27.9255536946904,-26.2727067131518));
#57576=CARTESIAN_POINT('Ctrl Pts',(-27.3216959316878,25.4490306024728,-26.1252300123211));
#57577=CARTESIAN_POINT('Ctrl Pts',(-27.4863078274828,23.8479932003446,-26.0440489486155));
#57578=CARTESIAN_POINT('Ctrl Pts',(-27.4835763998974,23.5538703223161,-26.0291635220347));
#57579=CARTESIAN_POINT('',(-27.4832525262206,23.5500450338769,-24.7791635219934));
#57580=CARTESIAN_POINT('Ctrl Pts',(-27.4832508680474,23.5538700228986,-26.0291635220347));
#57581=CARTESIAN_POINT('Ctrl Pts',(-27.4833559273522,23.4396477491317,-26.0233822513878));
#57582=CARTESIAN_POINT('Ctrl Pts',(-27.4784809167359,23.3252787802462,-26.0176009807409));
#57583=CARTESIAN_POINT('Ctrl Pts',(-27.4686142799239,23.2112389478804,-26.011819710094));
#57584=CARTESIAN_POINT('Ctrl Pts',(-27.4587552319999,23.0972868288391,-26.0060428860905));
#57585=CARTESIAN_POINT('Ctrl Pts',(-27.443912227658,22.9836637651824,-26.000266062087));
#57586=CARTESIAN_POINT('Ctrl Pts',(-27.4241257767461,22.8708446414902,-25.9944892380835));
#57587=CARTESIAN_POINT('Ctrl Pts',(-27.4043473789285,22.7580714352318,-25.9887147652499));
#57588=CARTESIAN_POINT('Ctrl Pts',(-27.3796296050901,22.6461019372493,-25.9829402924164));
#57589=CARTESIAN_POINT('Ctrl Pts',(-27.3500646256575,22.5354042422586,-25.9771658195828));
#57590=CARTESIAN_POINT('Ctrl Pts',(-27.3205040698356,22.4247231102257,-25.9713922107451));
#57591=CARTESIAN_POINT('Ctrl Pts',(-27.2860978596516,22.315313813927,-25.9656186019074));
#57592=CARTESIAN_POINT('Ctrl Pts',(-27.2469887198259,22.207631753009,-25.9598449930697));
#57593=CARTESIAN_POINT('Ctrl Pts',(-27.2078753655144,22.0999380880382,-25.9540707620554));
#57594=CARTESIAN_POINT('Ctrl Pts',(-27.1640582205472,21.9939724279231,-25.9482965310411));
#57595=CARTESIAN_POINT('Ctrl Pts',(-27.1157287660695,21.8901717438694,-25.9425223000268));
#57596=CARTESIAN_POINT('Ctrl Pts',(-27.0673511770414,21.7862676777415,-25.9367423180679));
#57597=CARTESIAN_POINT('Ctrl Pts',(-27.0144524833506,21.6845332802459,-25.930962336109));
#57598=CARTESIAN_POINT('Ctrl Pts',(-26.9572709229612,21.5853823880031,-25.9251823541501));
#57599=CARTESIAN_POINT('Ctrl Pts',(-26.9000607778477,21.4861819308155,-25.9193994828124));
#57600=CARTESIAN_POINT('Ctrl Pts',(-26.8385637324964,21.3895679085275,-25.9136166114747));
#57601=CARTESIAN_POINT('Ctrl Pts',(-26.7730612243053,21.2959248867343,-25.907833740137));
#57602=CARTESIAN_POINT('Ctrl Pts',(-26.7074515266995,21.202128625913,-25.9020414056106));
#57603=CARTESIAN_POINT('Ctrl Pts',(-26.6378235327476,21.1113134143342,-25.8962490710843));
#57604=CARTESIAN_POINT('Ctrl Pts',(-26.5644990173714,21.023830729306,-25.8904567365579));
#57605=CARTESIAN_POINT('Ctrl Pts',(-26.4989941395618,20.9456775691545,-25.8852821211726));
#57606=CARTESIAN_POINT('Ctrl Pts',(-26.4305398127726,20.870183700961,-25.8801075057874));
#57607=CARTESIAN_POINT('Ctrl Pts',(-26.359388676242,20.7975732693399,-25.8749328904021));
#57608=CARTESIAN_POINT('Ctrl Pts',(-26.2786443943463,20.715172938927,-25.8690605934334));
#57609=CARTESIAN_POINT('Ctrl Pts',(-26.1941361993304,20.6361902832086,-25.8631882964647));
#57610=CARTESIAN_POINT('Ctrl Pts',(-26.106185179249,20.5609888596232,-25.857315999496));
#57611=CARTESIAN_POINT('Ctrl Pts',(-26.0183481367047,20.4858848911104,-25.8514513125577));
#57612=CARTESIAN_POINT('Ctrl Pts',(-25.9270774529613,20.4145526762032,-25.8455866256195));
#57613=CARTESIAN_POINT('Ctrl Pts',(-25.8327320011325,20.3473200516702,-25.8397219386813));
#57614=CARTESIAN_POINT('Ctrl Pts',(-25.7384835776947,20.2801565716826,-25.8338632832065));
#57615=CARTESIAN_POINT('Ctrl Pts',(-25.6411670105871,20.2170845343467,-25.8280046277317));
#57616=CARTESIAN_POINT('Ctrl Pts',(-25.5411747747554,20.1583920360246,-25.8221459722568));
#57617=CARTESIAN_POINT('Ctrl Pts',(-25.4372767541204,20.0974069570225,-25.8160584725389));
#57618=CARTESIAN_POINT('Ctrl Pts',(-25.3304901211217,20.0411508246606,-25.809970972821));
#57619=CARTESIAN_POINT('Ctrl Pts',(-25.2212893627608,19.9898979272736,-25.8038834731031));
#57620=CARTESIAN_POINT('Ctrl Pts',(-25.116315452198,19.9406288823774,-25.7980316030197));
#57621=CARTESIAN_POINT('Ctrl Pts',(-25.0091112380853,19.8959831446882,-25.7921797329363));
#57622=CARTESIAN_POINT('Ctrl Pts',(-24.9001231887229,19.8561574856385,-25.7863278628529));
#57623=CARTESIAN_POINT('Ctrl Pts',(-24.7911517337818,19.8163378904076,-25.78047688377));
#57624=CARTESIAN_POINT('Ctrl Pts',(-24.6803973717949,19.7813370564274,-25.774625904687));
#57625=CARTESIAN_POINT('Ctrl Pts',(-24.5683251706689,19.7513030582514,-25.768774925604));
#57626=CARTESIAN_POINT('Ctrl Pts',(-24.4562428931736,19.72126635973,-25.7629234204617));
#57627=CARTESIAN_POINT('Ctrl Pts',(-24.3428429403163,19.6961974917576,-25.7570719153194));
#57628=CARTESIAN_POINT('Ctrl Pts',(-24.2286034146487,19.6761940551615,-25.7512204101771));
#57629=CARTESIAN_POINT('Ctrl Pts',(-24.1143259525213,19.6561839758595,-25.7453669618773));
#57630=CARTESIAN_POINT('Ctrl Pts',(-23.999208770172,19.6412427439838,-25.7395135135775));
#57631=CARTESIAN_POINT('Ctrl Pts',(-23.8837372728448,19.631416361679,-25.7336600652777));
#57632=CARTESIAN_POINT('Ctrl Pts',(-23.7681344593515,19.6215788046438,-25.7277999603362));
#57633=CARTESIAN_POINT('Ctrl Pts',(-23.6521769387767,19.6168677421984,-25.7219398553946));
#57634=CARTESIAN_POINT('Ctrl Pts',(-23.5363524188044,19.6172770948447,-25.7160797504531));
#57635=CARTESIAN_POINT('Ctrl Pts',(-23.420449898267,19.6176867231644,-25.7102156990976));
#57636=CARTESIAN_POINT('Ctrl Pts',(-23.304680968581,19.6232236130841,-25.7043516477422));
#57637=CARTESIAN_POINT('Ctrl Pts',(-23.1895287651332,19.6338297552006,-25.6984875963867));
#57638=CARTESIAN_POINT('Ctrl Pts',(-23.0742068503238,19.6444515286533,-25.6926149025901));
#57639=CARTESIAN_POINT('Ctrl Pts',(-22.9595038838278,19.6601574092395,-25.6867422087936));
#57640=CARTESIAN_POINT('Ctrl Pts',(-22.8458934457647,19.6808381989988,-25.680869514997));
#57641=CARTESIAN_POINT('Ctrl Pts',(-22.8147888082951,19.6865002532873,-25.6792616696737));
#57642=CARTESIAN_POINT('Ctrl Pts',(-22.7837659769105,19.6925349245322,-25.6776538243505));
#57643=CARTESIAN_POINT('Ctrl Pts',(-22.7528344570043,19.6989393252466,-25.6760459790272));
#57644=CARTESIAN_POINT('Ctrl Pts',(-22.6398639691377,19.7223299725667,-25.6701736820585));
#57645=CARTESIAN_POINT('Ctrl Pts',(-22.527734273729,19.7507346612045,-25.6643013850898));
#57646=CARTESIAN_POINT('Ctrl Pts',(-22.4169247994566,19.7840797726003,-25.6584290881211));
#57647=CARTESIAN_POINT('Ctrl Pts',(-22.3062589254623,19.8173816713799,-25.6525644011829));
#57648=CARTESIAN_POINT('Ctrl Pts',(-22.1969102624293,19.8556111428307,-25.6466997142447));
#57649=CARTESIAN_POINT('Ctrl Pts',(-22.0893486110632,19.8986434706521,-25.6408350273065));
#57650=CARTESIAN_POINT('Ctrl Pts',(-21.9818975801219,19.9416315424182,-25.6349763718317));
#57651=CARTESIAN_POINT('Ctrl Pts',(-21.8762302868094,19.9894124931336,-25.6291177163569));
#57652=CARTESIAN_POINT('Ctrl Pts',(-21.7728012607751,20.0418118553384,-25.6232590608821));
#57653=CARTESIAN_POINT('Ctrl Pts',(-21.6653322058849,20.0962579827837,-25.6171715611642));
#57654=CARTESIAN_POINT('Ctrl Pts',(-21.5602802757069,20.1556905444095,-25.6110840614463));
#57655=CARTESIAN_POINT('Ctrl Pts',(-21.4581327139585,20.2198586108137,-25.6049965617284));
#57656=CARTESIAN_POINT('Ctrl Pts',(-21.3599389910202,20.2815429156188,-25.599144691645));
#57657=CARTESIAN_POINT('Ctrl Pts',(-21.264429360388,20.3476027057622,-25.5932928215616));
#57658=CARTESIAN_POINT('Ctrl Pts',(-21.1720107042132,20.4177687232732,-25.5874409514782));
#57659=CARTESIAN_POINT('Ctrl Pts',(-21.0796061196191,20.48792405737,-25.5815899723952));
#57660=CARTESIAN_POINT('Ctrl Pts',(-20.9902919028745,20.5621841258165,-25.5757389933123));
#57661=CARTESIAN_POINT('Ctrl Pts',(-20.904444020505,20.6402376997528,-25.5698880142293));
#57662=CARTESIAN_POINT('Ctrl Pts',(-20.8185884195846,20.7182982914567,-25.564036509087));
#57663=CARTESIAN_POINT('Ctrl Pts',(-20.7362000784633,20.8001527885639,-25.5581850039447));
#57664=CARTESIAN_POINT('Ctrl Pts',(-20.657619545052,20.8854517127606,-25.5523334988024));
#57665=CARTESIAN_POINT('Ctrl Pts',(-20.5790129167564,20.9707789628729,-25.5464800505027));
#57666=CARTESIAN_POINT('Ctrl Pts',(-20.5042168904685,21.0595526106144,-25.5406266022029));
#57667=CARTESIAN_POINT('Ctrl Pts',(-20.4335325506769,21.1513891425185,-25.5347731539032));
#57668=CARTESIAN_POINT('Ctrl Pts',(-20.362767827442,21.2433301125014,-25.5289130489616));
#57669=CARTESIAN_POINT('Ctrl Pts',(-20.2961243759044,21.3383405911567,-25.5230529440201));
#57670=CARTESIAN_POINT('Ctrl Pts',(-20.2338607079589,21.4360069756005,-25.5171928390786));
#57671=CARTESIAN_POINT('Ctrl Pts',(-20.1715551093299,21.5337391322418,-25.5113287877231));
#57672=CARTESIAN_POINT('Ctrl Pts',(-20.1136353734299,21.6341303989133,-25.5054647363677));
#57673=CARTESIAN_POINT('Ctrl Pts',(-20.0603138511328,21.7367429491661,-25.4996006850122));
#57674=CARTESIAN_POINT('Ctrl Pts',(-20.0069137435559,21.8395067298343,-25.4937279912157));
#57675=CARTESIAN_POINT('Ctrl Pts',(-19.9581255484152,21.9444979543378,-25.4878552974191));
#57676=CARTESIAN_POINT('Ctrl Pts',(-19.9141133857657,22.0512591656495,-25.4819826036226));
#57677=CARTESIAN_POINT('Ctrl Pts',(-19.9020635918652,22.080488599411,-25.4803747582992));
#57678=CARTESIAN_POINT('Ctrl Pts',(-19.8903715065191,22.1098506236019,-25.4787669129758));
#57679=CARTESIAN_POINT('Ctrl Pts',(-19.8790398385043,22.1393356803663,-25.4771590676524));
#57680=CARTESIAN_POINT('Ctrl Pts',(-19.8376534446978,22.247023283732,-25.4712867706837));
#57681=CARTESIAN_POINT('Ctrl Pts',(-19.800939931946,22.3567138161882,-25.465414473715));
#57682=CARTESIAN_POINT('Ctrl Pts',(-19.7690965152443,22.4679641323916,-25.4595421767462));
#57683=CARTESIAN_POINT('Ctrl Pts',(-19.7372943650818,22.5790702770206,-25.453677489808));
#57684=CARTESIAN_POINT('Ctrl Pts',(-19.7103498728486,22.6917317918906,-25.4478128028698));
#57685=CARTESIAN_POINT('Ctrl Pts',(-19.6884120598263,22.8054860113383,-25.4419481159316));
#57686=CARTESIAN_POINT('Ctrl Pts',(-19.6664968084713,22.9191232416926,-25.4360894604568));
#57687=CARTESIAN_POINT('Ctrl Pts',(-19.6495780723987,23.0338505379084,-25.430230804982));
#57688=CARTESIAN_POINT('Ctrl Pts',(-19.6377547617519,23.1491911895073,-25.4243721495072));
#57689=CARTESIAN_POINT('Ctrl Pts',(-19.6254696221774,23.2690371485482,-25.4182846497892));
#57690=CARTESIAN_POINT('Ctrl Pts',(-19.6186862117189,23.3895449190781,-25.4121971500713));
#57691=CARTESIAN_POINT('Ctrl Pts',(-19.6174567951449,23.5101689368029,-25.4061096503534));
#57692=CARTESIAN_POINT('Ctrl Pts',(-19.6162749657563,23.6261239451599,-25.40025778027));
#57693=CARTESIAN_POINT('Ctrl Pts',(-19.6202251712741,23.7421859169408,-25.3944059101866));
#57694=CARTESIAN_POINT('Ctrl Pts',(-19.6293008175015,23.8578669900171,-25.3885540401033));
#57695=CARTESIAN_POINT('Ctrl Pts',(-19.6383750818792,23.9735304495979,-25.3827030610203));
#57696=CARTESIAN_POINT('Ctrl Pts',(-19.6525732029681,24.088812713784,-25.3768520819373));
#57697=CARTESIAN_POINT('Ctrl Pts',(-19.6718365645521,24.2032292432368,-25.3710011028544));
#57698=CARTESIAN_POINT('Ctrl Pts',(-19.6911016580977,24.3176560598371,-25.3651495977121));
#57699=CARTESIAN_POINT('Ctrl Pts',(-19.7154328288233,24.4312165792996,-25.3592980925698));
#57700=CARTESIAN_POINT('Ctrl Pts',(-19.7447201353424,24.5434353851088,-25.3534465874275));
#57701=CARTESIAN_POINT('Ctrl Pts',(-19.7740171675384,24.6556914563404,-25.3475931391277));
#57702=CARTESIAN_POINT('Ctrl Pts',(-19.8082735038125,24.7666045281894,-25.3417396908279));
#57703=CARTESIAN_POINT('Ctrl Pts',(-19.8473292367804,24.8757139879369,-25.3358862425282));
#57704=CARTESIAN_POINT('Ctrl Pts',(-19.8864293845975,24.9849475288328,-25.3300261375866));
#57705=CARTESIAN_POINT('Ctrl Pts',(-19.9303396836271,25.0923729742652,-25.3241660326451));
#57706=CARTESIAN_POINT('Ctrl Pts',(-19.9788518994618,25.1975492639468,-25.3183059277036));
#57707=CARTESIAN_POINT('Ctrl Pts',(-20.0273967852376,25.3027963832769,-25.3124418763481));
#57708=CARTESIAN_POINT('Ctrl Pts',(-20.080549569632,25.4057909644049,-25.3065778249927));
#57709=CARTESIAN_POINT('Ctrl Pts',(-20.1380566865571,25.5061176892215,-25.3007137736372));
#57710=CARTESIAN_POINT('Ctrl Pts',(-20.195648557493,25.6065922756033,-25.2948410798407));
#57711=CARTESIAN_POINT('Ctrl Pts',(-20.2576073484846,25.7043908104936,-25.2889683860441));
#57712=CARTESIAN_POINT('Ctrl Pts',(-20.3236369071072,25.7991279420206,-25.2830956922475));
#57713=CARTESIAN_POINT('Ctrl Pts',(-20.3417146957188,25.8250653838747,-25.2814878469242));
#57714=CARTESIAN_POINT('Ctrl Pts',(-20.3600973915214,25.8507735502683,-25.2798800016008));
#57715=CARTESIAN_POINT('Ctrl Pts',(-20.3787784175389,25.8762449958357,-25.2782721562774));
#57716=CARTESIAN_POINT('Ctrl Pts',(-20.4470067047137,25.9692737781571,-25.2723998593087));
#57717=CARTESIAN_POINT('Ctrl Pts',(-20.5194459800455,26.059453855328,-25.26652756234));
#57718=CARTESIAN_POINT('Ctrl Pts',(-20.5958300209873,26.1463797682195,-25.2606552653713));
#57719=CARTESIAN_POINT('Ctrl Pts',(-20.6721150742784,26.2331930320313,-25.2547905784331));
#57720=CARTESIAN_POINT('Ctrl Pts',(-20.7523344566912,26.3167602102763,-25.2489258914949));
#57721=CARTESIAN_POINT('Ctrl Pts',(-20.8361794721605,26.3967058384452,-25.2430612045567));
#57722=CARTESIAN_POINT('Ctrl Pts',(-20.91993825828,26.4765692475399,-25.2372025490819));
#57723=CARTESIAN_POINT('Ctrl Pts',(-21.0073149634256,26.5528182313041,-25.2313438936071));
#57724=CARTESIAN_POINT('Ctrl Pts',(-21.097961988199,26.6251118927519,-25.2254852381323));
#57725=CARTESIAN_POINT('Ctrl Pts',(-21.1921497656012,26.7002294082915,-25.2193977384144));
#57726=CARTESIAN_POINT('Ctrl Pts',(-21.2898682539351,26.7710759639824,-25.2133102386965));
#57727=CARTESIAN_POINT('Ctrl Pts',(-21.3906867121297,26.8373126879689,-25.2072227389786));
#57728=CARTESIAN_POINT('Ctrl Pts',(-21.4876027772966,26.9009855785613,-25.2013708688951));
#57729=CARTESIAN_POINT('Ctrl Pts',(-21.587382915016,26.9603986203455,-25.1955189988117));
#57730=CARTESIAN_POINT('Ctrl Pts',(-21.6896131142508,27.0152936509676,-25.1896671287283));
#57731=CARTESIAN_POINT('Ctrl Pts',(-21.7918277480081,27.0701803233221,-25.1838161496454));
#57732=CARTESIAN_POINT('Ctrl Pts',(-21.8964913374521,27.1205501567852,-25.1779651705624));
#57733=CARTESIAN_POINT('Ctrl Pts',(-22.0031645469578,27.1661905521094,-25.1721141914794));
#57734=CARTESIAN_POINT('Ctrl Pts',(-22.109847347412,27.2118350509445,-25.1662626863371));
#57735=CARTESIAN_POINT('Ctrl Pts',(-22.2185397470311,27.2527491037203,-25.1604111811948));
#57736=CARTESIAN_POINT('Ctrl Pts',(-22.328782341944,27.2887682231888,-25.1545596760525));
#57737=CARTESIAN_POINT('Ctrl Pts',(-22.4390615460226,27.3247993038227,-25.1487062277527));
#57738=CARTESIAN_POINT('Ctrl Pts',(-22.5508915762814,27.3559320906272,-25.1428527794529));
#57739=CARTESIAN_POINT('Ctrl Pts',(-22.6637984747916,27.3820521356663,-25.1369993311532));
#57740=CARTESIAN_POINT('Ctrl Pts',(-22.7768337729629,27.4082018848686,-25.1311392262116));
#57741=CARTESIAN_POINT('Ctrl Pts',(-22.8909479807313,27.4293274209012,-25.1252791212701));
#57742=CARTESIAN_POINT('Ctrl Pts',(-23.0056574671519,27.4453655230818,-25.1194190163285));
#57743=CARTESIAN_POINT('Ctrl Pts',(-23.1204442032322,27.4614144259204,-25.1135549649731));
#57744=CARTESIAN_POINT('Ctrl Pts',(-23.2358266056756,27.4723690339487,-25.1076909136176));
#57745=CARTESIAN_POINT('Ctrl Pts',(-23.3513181971683,27.478218179526,-25.1018268622621));
#57746=CARTESIAN_POINT('Ctrl Pts',(-23.4669800002124,27.4840759455763,-25.0959541684656));
#57747=CARTESIAN_POINT('Ctrl Pts',(-23.5827509016543,27.4848132292374,-25.090081474669));
#57748=CARTESIAN_POINT('Ctrl Pts',(-23.6981466155584,27.4804708894904,-25.0842087808724));
#57749=CARTESIAN_POINT('Ctrl Pts',(-23.7297400316901,27.4792820295061,-25.0826009355491));
#57750=CARTESIAN_POINT('Ctrl Pts',(-23.7613053697927,27.4777127128804,-25.0809930902258));
#57751=CARTESIAN_POINT('Ctrl Pts',(-23.7928328108208,27.4757644483974,-25.0793852449025));
#57752=CARTESIAN_POINT('Ctrl Pts',(-23.9079797678678,27.468648846261,-25.0735129479338));
#57753=CARTESIAN_POINT('Ctrl Pts',(-24.0230062790909,27.456450623236,-25.0676406509651));
#57754=CARTESIAN_POINT('Ctrl Pts',(-24.1374273203492,27.4391745889702,-25.0617683539964));
#57755=CARTESIAN_POINT('Ctrl Pts',(-24.2517000810251,27.4219209430728,-25.0559036670582));
#57756=CARTESIAN_POINT('Ctrl Pts',(-24.3653685271285,27.3996026332139,-25.05003898012));
#57757=CARTESIAN_POINT('Ctrl Pts',(-24.4779499107581,27.3722764160882,-25.0441742931818));
#57758=CARTESIAN_POINT('Ctrl Pts',(-24.5904155114828,27.344978302266,-25.038315637707));
#57759=CARTESIAN_POINT('Ctrl Pts',(-24.7017958741413,27.3126826223473,-25.0324569822321));
#57760=CARTESIAN_POINT('Ctrl Pts',(-24.811616304169,27.2754975482653,-25.0265983267573));
#57761=CARTESIAN_POINT('Ctrl Pts',(-24.9257264169218,27.2368599924377,-25.0205108270394));
#57762=CARTESIAN_POINT('Ctrl Pts',(-25.0381517984308,27.1929433554071,-25.0144233273215));
#57763=CARTESIAN_POINT('Ctrl Pts',(-25.1483745163087,27.1439268522597,-25.0083358276036));
#57764=CARTESIAN_POINT('Ctrl Pts',(-25.2543308292697,27.0968076372038,-25.0024839575202));
#57765=CARTESIAN_POINT('Ctrl Pts',(-25.3582514125868,27.0449762009867,-24.9966320874368));
#57766=CARTESIAN_POINT('Ctrl Pts',(-25.4596952794236,26.9886413103438,-24.9907802173534));
#57767=CARTESIAN_POINT('Ctrl Pts',(-25.5611237005096,26.9323149972,-24.9849292382704));
#57768=CARTESIAN_POINT('Ctrl Pts',(-25.6600757936188,26.8714867936446,-24.9790782591874));
#57769=CARTESIAN_POINT('Ctrl Pts',(-25.7561352159074,26.8064114012041,-24.9732272801044));
#57770=CARTESIAN_POINT('Ctrl Pts',(-25.8522032748621,26.7413301578599,-24.9673757749621));
#57771=CARTESIAN_POINT('Ctrl Pts',(-25.9453778037202,26.6720011983877,-24.9615242698198));
#57772=CARTESIAN_POINT('Ctrl Pts',(-26.0352720893322,26.5987221146418,-24.9556727646776));
#57773=CARTESIAN_POINT('Ctrl Pts',(-26.1251962268789,26.5254186965079,-24.9498193163778));
#57774=CARTESIAN_POINT('Ctrl Pts',(-26.2118376349368,26.4481628068202,-24.9439658680781));
#57775=CARTESIAN_POINT('Ctrl Pts',(-26.2948438321841,26.3672913303754,-24.9381124197784));
#57776=CARTESIAN_POINT('Ctrl Pts',(-26.3779444255028,26.2863278855003,-24.9322523148368));
#57777=CARTESIAN_POINT('Ctrl Pts',(-26.4574012603598,26.2017409356693,-24.9263922098953));
#57778=CARTESIAN_POINT('Ctrl Pts',(-26.5328997251062,26.1139031942518,-24.9205321049538));
#57779=CARTESIAN_POINT('Ctrl Pts',(-26.6084490333431,26.026006299613,-24.9146680535983));
#57780=CARTESIAN_POINT('Ctrl Pts',(-26.6800344088042,25.9348545785614,-24.9088040022429));
#57781=CARTESIAN_POINT('Ctrl Pts',(-26.7473834943546,25.8408512760399,-24.9029399508875));
#57782=CARTESIAN_POINT('Ctrl Pts',(-26.8148318390131,25.7467094314152,-24.8970672570909));
#57783=CARTESIAN_POINT('Ctrl Pts',(-26.8780312082338,25.6497079626739,-24.8911945632943));
#57784=CARTESIAN_POINT('Ctrl Pts',(-26.9367542002845,25.5502763937106,-24.8853218694978));
#57785=CARTESIAN_POINT('Ctrl Pts',(-26.9528315731928,25.5230536934146,-24.8837140241744));
#57786=CARTESIAN_POINT('Ctrl Pts',(-26.9685736841801,25.4956489626921,-24.882106178851));
#57787=CARTESIAN_POINT('Ctrl Pts',(-26.9839764950017,25.4680712780328,-24.8804983335276));
#57788=CARTESIAN_POINT('Ctrl Pts',(-27.0428859532857,25.3625979015933,-24.8743489820812));
#57789=CARTESIAN_POINT('Ctrl Pts',(-27.0970105455507,25.2542673935842,-24.8681996306348));
#57790=CARTESIAN_POINT('Ctrl Pts',(-27.1460768847945,25.1435309824525,-24.8620502791883));
#57791=CARTESIAN_POINT('Ctrl Pts',(-27.1950567706787,25.032989685424,-24.8559117627074));
#57792=CARTESIAN_POINT('Ctrl Pts',(-27.238996010439,24.9200512530229,-24.8497732462264));
#57793=CARTESIAN_POINT('Ctrl Pts',(-27.2776665386152,24.8051922995753,-24.8436347297455));
#57794=CARTESIAN_POINT('Ctrl Pts',(-27.3162505695764,24.6905902595975,-24.8375099437359));
#57795=CARTESIAN_POINT('Ctrl Pts',(-27.3495892676818,24.5740765989749,-24.8313851577262));
#57796=CARTESIAN_POINT('Ctrl Pts',(-27.3775025586027,24.4561477969037,-24.8252603717166));
#57797=CARTESIAN_POINT('Ctrl Pts',(-27.4053783968587,24.3383772258314,-24.8191438036401));
#57798=CARTESIAN_POINT('Ctrl Pts',(-27.4278432409376,24.2191956400605,-24.8130272355637));
#57799=CARTESIAN_POINT('Ctrl Pts',(-27.4447663970275,24.0991156774114,-24.8069106674872));
#57800=CARTESIAN_POINT('Ctrl Pts',(-27.4616615688625,23.9792342798678,-24.8008042138124));
#57801=CARTESIAN_POINT('Ctrl Pts',(-27.4730332684047,23.8584578192019,-24.7946977601377));
#57802=CARTESIAN_POINT('Ctrl Pts',(-27.4788017190277,23.7373094286559,-24.788591306463));
#57803=CARTESIAN_POINT('Ctrl Pts',(-27.4817703656354,23.6749622262403,-24.7854487116536));
#57804=CARTESIAN_POINT('Ctrl Pts',(-27.4832558220972,23.6125166982619,-24.7823061168441));
#57805=CARTESIAN_POINT('Ctrl Pts',(-27.4832525262206,23.5500450346982,-24.7791635220347));
#57806=CARTESIAN_POINT('',(-27.4832509332757,23.5467066668166,-23.5291635220347));
#57807=CARTESIAN_POINT('Ctrl Pts',(-27.4832525262206,23.5500450338768,-24.7791635219934));
#57808=CARTESIAN_POINT('Ctrl Pts',(-27.483246071975,23.4277085761306,-24.7730094691767));
#57809=CARTESIAN_POINT('Ctrl Pts',(-27.4775273894719,23.3054919752915,-24.76685541636));
#57810=CARTESIAN_POINT('Ctrl Pts',(-27.466155630688,23.1839303793606,-24.7607013635433));
#57811=CARTESIAN_POINT('Ctrl Pts',(-27.4547662630801,23.0621805489794,-24.7545377813622));
#57812=CARTESIAN_POINT('Ctrl Pts',(-27.4377063854403,22.9410880911425,-24.7483741991811));
#57813=CARTESIAN_POINT('Ctrl Pts',(-27.4150864501085,22.8211792959528,-24.742210617));
#57814=CARTESIAN_POINT('Ctrl Pts',(-27.3924085127843,22.7009630308734,-24.7360312301739));
#57815=CARTESIAN_POINT('Ctrl Pts',(-27.3641420805642,22.5819368368814,-24.7298518433478));
#57816=CARTESIAN_POINT('Ctrl Pts',(-27.3304482090873,22.4646146359764,-24.7236724565217));
#57817=CARTESIAN_POINT('Ctrl Pts',(-27.2967063493928,22.3471253398976,-24.7174842687551));
#57818=CARTESIAN_POINT('Ctrl Pts',(-27.2575217357048,22.2313452068291,-24.7112960809885));
#57819=CARTESIAN_POINT('Ctrl Pts',(-27.2131038988971,22.1177690721807,-24.7051078932219));
#57820=CARTESIAN_POINT('Ctrl Pts',(-27.1685852853359,22.0039352519955,-24.6989056654767));
#57821=CARTESIAN_POINT('Ctrl Pts',(-27.1188098567107,21.8923157411691,-24.6927034377316));
#57822=CARTESIAN_POINT('Ctrl Pts',(-27.0640340105662,21.7833827802026,-24.6865012099865));
#57823=CARTESIAN_POINT('Ctrl Pts',(-27.049639061038,21.7547554821242,-24.6848712807086));
#57824=CARTESIAN_POINT('Ctrl Pts',(-27.034899004807,21.7263135716238,-24.6832413514307));
#57825=CARTESIAN_POINT('Ctrl Pts',(-27.0198189886844,21.6980652839981,-24.6816114221528));
#57826=CARTESIAN_POINT('Ctrl Pts',(-26.9654888197847,21.5962925653642,-24.6757391251841));
#57827=CARTESIAN_POINT('Ctrl Pts',(-26.9065858911063,21.4967418751502,-24.6698668282154));
#57828=CARTESIAN_POINT('Ctrl Pts',(-26.8433161667284,21.3998523606526,-24.6639945312467));
#57829=CARTESIAN_POINT('Ctrl Pts',(-26.7801284348885,21.3030884072711,-24.6581298443086));
#57830=CARTESIAN_POINT('Ctrl Pts',(-26.7125853850435,21.2089791143613,-24.6522651573704));
#57831=CARTESIAN_POINT('Ctrl Pts',(-26.6409392828495,21.1179399682614,-24.6464004704322));
#57832=CARTESIAN_POINT('Ctrl Pts',(-26.5693668641865,21.0269944502241,-24.6405418149575));
#57833=CARTESIAN_POINT('Ctrl Pts',(-26.4937000405536,20.9391131215564,-24.6346831594827));
#57834=CARTESIAN_POINT('Ctrl Pts',(-26.4142344943633,20.8546827742021,-24.6288245040079));
#57835=CARTESIAN_POINT('Ctrl Pts',(-26.3316649539457,20.7669545031141,-24.62273700429));
#57836=CARTESIAN_POINT('Ctrl Pts',(-26.2449941268371,20.6829526868011,-24.6166495045721));
#57837=CARTESIAN_POINT('Ctrl Pts',(-26.1546002825104,20.6030739159977,-24.6105620048541));
#57838=CARTESIAN_POINT('Ctrl Pts',(-26.0677053243423,20.5262870230496,-24.6047101347708));
#57839=CARTESIAN_POINT('Ctrl Pts',(-25.9773705431083,20.4533102273088,-24.5988582646874));
#57840=CARTESIAN_POINT('Ctrl Pts',(-25.8839691058204,20.3844578523682,-24.593006394604));
#57841=CARTESIAN_POINT('Ctrl Pts',(-25.7905818897506,20.3156159608278,-24.5871554155211));
#57842=CARTESIAN_POINT('Ctrl Pts',(-25.6941292786793,20.2508974866819,-24.5813044364382));
#57843=CARTESIAN_POINT('Ctrl Pts',(-25.5950159761787,20.1905752471771,-24.5754534573552));
#57844=CARTESIAN_POINT('Ctrl Pts',(-25.4958937624383,20.1302475841225,-24.5696019522129));
#57845=CARTESIAN_POINT('Ctrl Pts',(-25.394110734862,20.0743171563871,-24.5637504470707));
#57846=CARTESIAN_POINT('Ctrl Pts',(-25.2900982923399,20.0230120055657,-24.5578989419284));
#57847=CARTESIAN_POINT('Ctrl Pts',(-25.1860513095499,19.9716898174205,-24.5520454936287));
#57848=CARTESIAN_POINT('Ctrl Pts',(-25.0797738102331,19.9249961431086,-24.5461920453289));
#57849=CARTESIAN_POINT('Ctrl Pts',(-24.9717187038767,19.8831115579463,-24.5403385970292));
#57850=CARTESIAN_POINT('Ctrl Pts',(-24.8635407154007,19.8411793409156,-24.5344784920877));
#57851=CARTESIAN_POINT('Ctrl Pts',(-24.7535814706499,19.8040672784442,-24.5286183871461));
#57852=CARTESIAN_POINT('Ctrl Pts',(-24.6423107267535,19.7719066107119,-24.5227582822046));
#57853=CARTESIAN_POINT('Ctrl Pts',(-24.5309650489753,19.7397242847827,-24.5168942308492));
#57854=CARTESIAN_POINT('Ctrl Pts',(-24.4183065142351,19.7125000900164,-24.5110301794938));
#57855=CARTESIAN_POINT('Ctrl Pts',(-24.3048150870377,19.6903141448707,-24.5051661281384));
#57856=CARTESIAN_POINT('Ctrl Pts',(-24.1911563961316,19.6680955020706,-24.4992934343418));
#57857=CARTESIAN_POINT('Ctrl Pts',(-24.0766627701595,19.6509299895671,-24.4934207405453));
#57858=CARTESIAN_POINT('Ctrl Pts',(-23.9618193905294,19.6388459150525,-24.4875480467488));
#57859=CARTESIAN_POINT('Ctrl Pts',(-23.9303771942756,19.6355374975916,-24.4859402014251));
#57860=CARTESIAN_POINT('Ctrl Pts',(-23.8989087792088,19.6326096694182,-24.4843323561015));
#57861=CARTESIAN_POINT('Ctrl Pts',(-23.8674240791189,19.6300623310146,-24.4827245107778));
#57862=CARTESIAN_POINT('Ctrl Pts',(-23.7524332238541,19.6207587448015,-24.4768522138091));
#57863=CARTESIAN_POINT('Ctrl Pts',(-23.6368400278673,19.6165033986725,-24.4709799168404));
#57864=CARTESIAN_POINT('Ctrl Pts',(-23.5211252854633,19.6173603893228,-24.4651076198717));
#57865=CARTESIAN_POINT('Ctrl Pts',(-23.4055605001756,19.6182162693812,-24.4592429329335));
#57866=CARTESIAN_POINT('Ctrl Pts',(-23.2898748912665,19.624171308076,-24.4533782459953));
#57867=CARTESIAN_POINT('Ctrl Pts',(-23.1745543746449,19.6352378580576,-24.4475135590571));
#57868=CARTESIAN_POINT('Ctrl Pts',(-23.0593524579555,19.6462930267854,-24.4416549035823));
#57869=CARTESIAN_POINT('Ctrl Pts',(-22.9445152957341,19.6624492113657,-24.4357962481075));
#57870=CARTESIAN_POINT('Ctrl Pts',(-22.8305281314116,19.683666726667,-24.4299375926326));
#57871=CARTESIAN_POINT('Ctrl Pts',(-22.7120885280519,19.7057130168041,-24.4238500929147));
#57872=CARTESIAN_POINT('Ctrl Pts',(-22.5945671342954,19.7332240950283,-24.4177625931968));
#57873=CARTESIAN_POINT('Ctrl Pts',(-22.4785020792672,19.7660960909901,-24.4116750934789));
#57874=CARTESIAN_POINT('Ctrl Pts',(-22.3669295692514,19.7976957063764,-24.4058232233955));
#57875=CARTESIAN_POINT('Ctrl Pts',(-22.2567031877513,19.8342488216843,-24.3999713533121));
#57876=CARTESIAN_POINT('Ctrl Pts',(-22.148289093069,19.8756113904726,-24.3941194832287));
#57877=CARTESIAN_POINT('Ctrl Pts',(-22.0398915054184,19.9169676614338,-24.3882685041458));
#57878=CARTESIAN_POINT('Ctrl Pts',(-21.933306042056,19.9631317825476,-24.3824175250628));
#57879=CARTESIAN_POINT('Ctrl Pts',(-21.828980988146,20.0139107391958,-24.3765665459798));
#57880=CARTESIAN_POINT('Ctrl Pts',(-21.7246465544096,20.0646942613608,-24.3707150408375));
#57881=CARTESIAN_POINT('Ctrl Pts',(-21.6225733058471,20.120093262952,-24.3648635356952));
#57882=CARTESIAN_POINT('Ctrl Pts',(-21.5231862870665,20.1798680669942,-24.359012030553));
#57883=CARTESIAN_POINT('Ctrl Pts',(-21.4237662640206,20.2396627209476,-24.3531585822532));
#57884=CARTESIAN_POINT('Ctrl Pts',(-21.3270345985799,20.3038358538226,-24.3473051339534));
#57885=CARTESIAN_POINT('Ctrl Pts',(-21.2333880285658,20.3721040338824,-24.3414516856536));
#57886=CARTESIAN_POINT('Ctrl Pts',(-21.1396349620668,20.440449849687,-24.3355915807121));
#57887=CARTESIAN_POINT('Ctrl Pts',(-21.0489743279428,20.5128997641621,-24.3297314757706));
#57888=CARTESIAN_POINT('Ctrl Pts',(-20.9617704644022,20.5891295036341,-24.323871370829));
#57889=CARTESIAN_POINT('Ctrl Pts',(-20.8745078745173,20.6654105790646,-24.3180073194736));
#57890=CARTESIAN_POINT('Ctrl Pts',(-20.7907069887246,20.7454762631683,-24.3121432681181));
#57891=CARTESIAN_POINT('Ctrl Pts',(-20.7106946531889,20.8289660611772,-24.3062792167627));
#57892=CARTESIAN_POINT('Ctrl Pts',(-20.6305643954427,20.9125789064823,-24.3004065229661));
#57893=CARTESIAN_POINT('Ctrl Pts',(-20.554234103199,20.9996256278098,-24.2945338291696));
#57894=CARTESIAN_POINT('Ctrl Pts',(-20.4819898533138,21.0897133354086,-24.288661135373));
#57895=CARTESIAN_POINT('Ctrl Pts',(-20.4622105861936,21.1143778427662,-24.2870532900497));
#57896=CARTESIAN_POINT('Ctrl Pts',(-20.4427373428466,21.1392701330953,-24.2854454447263));
#57897=CARTESIAN_POINT('Ctrl Pts',(-20.4235754091814,21.1643817951381,-24.2838375994029));
#57898=CARTESIAN_POINT('Ctrl Pts',(-20.3535907139232,21.2560965482624,-24.2779653024342));
#57899=CARTESIAN_POINT('Ctrl Pts',(-20.2875275970532,21.3510468485179,-24.2720930054655));
#57900=CARTESIAN_POINT('Ctrl Pts',(-20.2256998739005,21.4488628425701,-24.2662207084968));
#57901=CARTESIAN_POINT('Ctrl Pts',(-20.1639522745668,21.5465520748624,-24.2603560215586));
#57902=CARTESIAN_POINT('Ctrl Pts',(-20.1064293726592,21.6470992695062,-24.2544913346203));
#57903=CARTESIAN_POINT('Ctrl Pts',(-20.0534042188184,21.7501022944257,-24.2486266476821));
#57904=CARTESIAN_POINT('Ctrl Pts',(-20.0004335980289,21.8529993871822,-24.2427679922073));
#57905=CARTESIAN_POINT('Ctrl Pts',(-19.9519517127152,21.9583469212006,-24.2369093367325));
#57906=CARTESIAN_POINT('Ctrl Pts',(-19.9081874697557,22.0657152015449,-24.2310506812576));
#57907=CARTESIAN_POINT('Ctrl Pts',(-19.8627137569192,22.1772773814879,-24.2249631815397));
#57908=CARTESIAN_POINT('Ctrl Pts',(-19.8223339932062,22.2910210059157,-24.2188756818218));
#57909=CARTESIAN_POINT('Ctrl Pts',(-19.7872516723537,22.4064371914391,-24.2127881821039));
#57910=CARTESIAN_POINT('Ctrl Pts',(-19.7535272874064,22.5173859478259,-24.2069363120205));
#57911=CARTESIAN_POINT('Ctrl Pts',(-19.7246980045834,22.6298797604081,-24.2010844419371));
#57912=CARTESIAN_POINT('Ctrl Pts',(-19.700894613521,22.7434485791769,-24.1952325718537));
#57913=CARTESIAN_POINT('Ctrl Pts',(-19.6770948467414,22.8570001060604,-24.1893815927707));
#57914=CARTESIAN_POINT('Ctrl Pts',(-19.6583195349616,22.9716259092027,-24.1835306136877));
#57915=CARTESIAN_POINT('Ctrl Pts',(-19.6446486088804,23.08684450619,-24.1776796346047));
#57916=CARTESIAN_POINT('Ctrl Pts',(-19.6309764536514,23.2020734624381,-24.1718281294624));
#57917=CARTESIAN_POINT('Ctrl Pts',(-19.6224096451481,23.3178949079546,-24.1659766243201));
#57918=CARTESIAN_POINT('Ctrl Pts',(-19.6189762937397,23.4338216900134,-24.1601251191778));
#57919=CARTESIAN_POINT('Ctrl Pts',(-19.61554180219,23.5497869688329,-24.154271670878));
#57920=CARTESIAN_POINT('Ctrl Pts',(-19.6172441696736,23.6658572407673,-24.1484182225783));
#57921=CARTESIAN_POINT('Ctrl Pts',(-19.6240593939259,23.7815455167614,-24.1425647742785));
#57922=CARTESIAN_POINT('Ctrl Pts',(-19.6308823685682,23.8973653554466,-24.1367046693369));
#57923=CARTESIAN_POINT('Ctrl Pts',(-19.6428297810778,24.0128019182055,-24.1308445643954));
#57924=CARTESIAN_POINT('Ctrl Pts',(-19.6598257548193,24.1273733975231,-24.1249844594538));
#57925=CARTESIAN_POINT('Ctrl Pts',(-19.6768331742854,24.2420220335613,-24.1191204080984));
#57926=CARTESIAN_POINT('Ctrl Pts',(-19.6988958463412,24.3558040212941,-24.1132563567429));
#57927=CARTESIAN_POINT('Ctrl Pts',(-19.7258871548982,24.4682495168548,-24.1073923053874));
#57928=CARTESIAN_POINT('Ctrl Pts',(-19.752918243256,24.5808607346297,-24.1015196115908));
#57929=CARTESIAN_POINT('Ctrl Pts',(-19.784892351572,24.692131133233,-24.0956469177943));
#57930=CARTESIAN_POINT('Ctrl Pts',(-19.8216335717749,24.8016076578396,-24.0897742239977));
#57931=CARTESIAN_POINT('Ctrl Pts',(-19.8316927032601,24.831580498956,-24.0881663786745));
#57932=CARTESIAN_POINT('Ctrl Pts',(-19.8421088912036,24.86141900349,-24.0865585333513));
#57933=CARTESIAN_POINT('Ctrl Pts',(-19.8528779163308,24.8911141776766,-24.0849506880281));
#57934=CARTESIAN_POINT('Ctrl Pts',(-19.8922093822981,24.9995691881455,-24.0790783910594));
#57935=CARTESIAN_POINT('Ctrl Pts',(-19.93638274772,25.1064738593082,-24.0732060940907));
#57936=CARTESIAN_POINT('Ctrl Pts',(-19.9852564792695,25.2113642516566,-24.067333797122));
#57937=CARTESIAN_POINT('Ctrl Pts',(-20.0340668743444,25.3161187143867,-24.0614691101838));
#57938=CARTESIAN_POINT('Ctrl Pts',(-20.0875653491538,25.4188637180978,-24.0556044232456));
#57939=CARTESIAN_POINT('Ctrl Pts',(-20.1455611786818,25.5191521712702,-24.0497397363074));
#57940=CARTESIAN_POINT('Ctrl Pts',(-20.2034973631297,25.6193374840466,-24.0438810808325));
#57941=CARTESIAN_POINT('Ctrl Pts',(-20.265921496741,25.7170709157377,-24.0380224253577));
#57942=CARTESIAN_POINT('Ctrl Pts',(-20.3325958038284,25.8119276148173,-24.0321637698829));
#57943=CARTESIAN_POINT('Ctrl Pts',(-20.4018744680766,25.9104895001116,-24.026076270165));
#57944=CARTESIAN_POINT('Ctrl Pts',(-20.4757419136197,26.005944923763,-24.0199887704471));
#57945=CARTESIAN_POINT('Ctrl Pts',(-20.5538800053159,26.0978476100309,-24.0139012707292));
#57946=CARTESIAN_POINT('Ctrl Pts',(-20.6289935958473,26.1861930072016,-24.0080494006458));
#57947=CARTESIAN_POINT('Ctrl Pts',(-20.7080530782955,26.2712552411972,-24.0021975305624));
#57948=CARTESIAN_POINT('Ctrl Pts',(-20.7907336890445,26.3526701945455,-23.996345660479));
#57949=CARTESIAN_POINT('Ctrl Pts',(-20.8734017109186,26.4340727517269,-23.9904946813961));
#57950=CARTESIAN_POINT('Ctrl Pts',(-20.959689470363,26.511828842475,-23.9846437023131));
#57951=CARTESIAN_POINT('Ctrl Pts',(-21.0492350940756,26.5856109580958,-23.9787927232302));
#57952=CARTESIAN_POINT('Ctrl Pts',(-21.1387887688015,26.659399707439,-23.9729412180879));
#57953=CARTESIAN_POINT('Ctrl Pts',(-21.2316005710262,26.7292135084901,-23.9670897129456));
#57954=CARTESIAN_POINT('Ctrl Pts',(-21.3272758458338,26.7947653848235,-23.9612382078033));
#57955=CARTESIAN_POINT('Ctrl Pts',(-21.4229828923173,26.860339029508,-23.9553847595035));
#57956=CARTESIAN_POINT('Ctrl Pts',(-21.5215549613443,26.9216477017299,-23.9495313112038));
#57957=CARTESIAN_POINT('Ctrl Pts',(-21.6225693666104,26.9784483567679,-23.943677862904));
#57958=CARTESIAN_POINT('Ctrl Pts',(-21.7236986471903,27.0353136064847,-23.9378177579625));
#57959=CARTESIAN_POINT('Ctrl Pts',(-21.8272754472104,27.0876604037582,-23.931957653021));
#57960=CARTESIAN_POINT('Ctrl Pts',(-21.9328533993863,27.1352921474878,-23.9260975480794));
#57961=CARTESIAN_POINT('Ctrl Pts',(-22.038502451705,27.1829559682157,-23.920233496724));
#57962=CARTESIAN_POINT('Ctrl Pts',(-22.1461549565958,27.2258982599727,-23.9143694453686));
#57963=CARTESIAN_POINT('Ctrl Pts',(-22.2553471851667,27.2639715764705,-23.9085053940131));
#57964=CARTESIAN_POINT('Ctrl Pts',(-22.3647003412857,27.3021010054367,-23.9026327002166));
#57965=CARTESIAN_POINT('Ctrl Pts',(-22.475597355576,27.3353470191732,-23.89676000642));
#57966=CARTESIAN_POINT('Ctrl Pts',(-22.5875619796419,27.3636127167527,-23.8908873126234));
#57967=CARTESIAN_POINT('Ctrl Pts',(-22.6182160207729,27.3713513919228,-23.8892794673));
#57968=CARTESIAN_POINT('Ctrl Pts',(-22.6489500464356,27.3787170548861,-23.8876716219767));
#57969=CARTESIAN_POINT('Ctrl Pts',(-22.6797542093278,27.3857083938776,-23.8860637766533));
#57970=CARTESIAN_POINT('Ctrl Pts',(-22.7922595540549,27.411242702539,-23.8801914796846));
#57971=CARTESIAN_POINT('Ctrl Pts',(-22.9060778242296,27.4318654158321,-23.8743191827158));
#57972=CARTESIAN_POINT('Ctrl Pts',(-23.0207421949965,27.4474448291476,-23.8684468857471));
#57973=CARTESIAN_POINT('Ctrl Pts',(-23.1352579698452,27.4630040527807,-23.8625821988089));
#57974=CARTESIAN_POINT('Ctrl Pts',(-23.2506172589443,27.4735329184887,-23.8567175118707));
#57975=CARTESIAN_POINT('Ctrl Pts',(-23.3663408217403,27.4789502145074,-23.8508528249325));
#57976=CARTESIAN_POINT('Ctrl Pts',(-23.4819453700963,27.4843619391763,-23.8449941694577));
#57977=CARTESIAN_POINT('Ctrl Pts',(-23.5979130365375,27.4846725312448,-23.8391355139829));
#57978=CARTESIAN_POINT('Ctrl Pts',(-23.7137578585075,27.4798523851276,-23.8332768585081));
#57979=CARTESIAN_POINT('Ctrl Pts',(-23.8341276812585,27.4748439598575,-23.8271893587902));
#57980=CARTESIAN_POINT('Ctrl Pts',(-23.9543644165304,27.464295741682,-23.8211018590723));
#57981=CARTESIAN_POINT('Ctrl Pts',(-24.0739206395242,27.4482341520769,-23.8150143593543));
#57982=CARTESIAN_POINT('Ctrl Pts',(-24.1888491844183,27.4327942604865,-23.8091624892709));
#57983=CARTESIAN_POINT('Ctrl Pts',(-24.3031484709066,27.4122599349419,-23.8033106191875));
#57984=CARTESIAN_POINT('Ctrl Pts',(-24.4163366123485,27.3867075835927,-23.7974587491042));
#57985=CARTESIAN_POINT('Ctrl Pts',(-24.5295075198667,27.3611591228212,-23.7916077700212));
#57986=CARTESIAN_POINT('Ctrl Pts',(-24.6415672156015,27.3305942464073,-23.7857567909382));
#57987=CARTESIAN_POINT('Ctrl Pts',(-24.7520445531331,27.2951403720982,-23.7799058118553));
#57988=CARTESIAN_POINT('Ctrl Pts',(-24.8625318236407,27.2596833101446,-23.774054306713));
#57989=CARTESIAN_POINT('Ctrl Pts',(-24.9714360594924,27.2193365027986,-23.7682028015706));
#57990=CARTESIAN_POINT('Ctrl Pts',(-25.0783024948938,27.174276856939,-23.7623512964283));
#57991=CARTESIAN_POINT('Ctrl Pts',(-25.1852044183119,27.1292022477519,-23.7564978481286));
#57992=CARTESIAN_POINT('Ctrl Pts',(-25.2900668149801,27.0794118486079,-23.7506443998288));
#57993=CARTESIAN_POINT('Ctrl Pts',(-25.39245672743,27.0251298966113,-23.744790951529));
#57994=CARTESIAN_POINT('Ctrl Pts',(-25.494963079444,26.9707862142482,-23.7389308465875));
#57995=CARTESIAN_POINT('Ctrl Pts',(-25.5949909696208,26.9119409776187,-23.7330707416459));
#57996=CARTESIAN_POINT('Ctrl Pts',(-25.6921337137158,26.8488634517788,-23.7272106367044));
#57997=CARTESIAN_POINT('Ctrl Pts',(-25.7893418773691,26.7857434471732,-23.7213465853489));
#57998=CARTESIAN_POINT('Ctrl Pts',(-25.8836606905278,26.7183857177358,-23.7154825339935));
#57999=CARTESIAN_POINT('Ctrl Pts',(-25.9747154390308,26.6471007053942,-23.709618482638));
#58000=CARTESIAN_POINT('Ctrl Pts',(-26.0659043840567,26.5757106331743,-23.7037457888415));
#58001=CARTESIAN_POINT('Ctrl Pts',(-26.1538193507051,26.5003819942174,-23.6978730950449));
#58002=CARTESIAN_POINT('Ctrl Pts',(-26.2381213821525,26.4214630852301,-23.6920004012483));
#58003=CARTESIAN_POINT('Ctrl Pts',(-26.2612018681621,26.3998564081015,-23.690392555925));
#58004=CARTESIAN_POINT('Ctrl Pts',(-26.2840117677736,26.3779808097334,-23.6887847106017));
#58005=CARTESIAN_POINT('Ctrl Pts',(-26.3065446544932,26.3558438657619,-23.6871768652783));
#58006=CARTESIAN_POINT('Ctrl Pts',(-26.3876711510968,26.2761429054605,-23.6813880438199));
#58007=CARTESIAN_POINT('Ctrl Pts',(-26.4654924669509,26.1927680362001,-23.6755992223615));
#58008=CARTESIAN_POINT('Ctrl Pts',(-26.5396500511236,26.1060286312048,-23.6698104009031));
#58009=CARTESIAN_POINT('Ctrl Pts',(-26.614723138346,26.0182183958866,-23.6639501142836));
#58010=CARTESIAN_POINT('Ctrl Pts',(-26.6860410514383,25.9269602310897,-23.6580898276641));
#58011=CARTESIAN_POINT('Ctrl Pts',(-26.7532673635898,25.8326164349,-23.6522295410446));
#58012=CARTESIAN_POINT('Ctrl Pts',(-26.8195082059408,25.7396556234232,-23.6464551603048));
#58013=CARTESIAN_POINT('Ctrl Pts',(-26.8817763186912,25.6436993807576,-23.640680779565));
#58014=CARTESIAN_POINT('Ctrl Pts',(-26.9397886290073,25.5451294815363,-23.6349063988252));
#58015=CARTESIAN_POINT('Ctrl Pts',(-26.997763743313,25.4466227828146,-23.6291357204707));
#58016=CARTESIAN_POINT('Ctrl Pts',(-27.051488261838,25.3455061234113,-23.6233650421162));
#58017=CARTESIAN_POINT('Ctrl Pts',(-27.1007222013158,25.242190510787,-23.6175943637617));
#58018=CARTESIAN_POINT('Ctrl Pts',(-27.149937291019,25.1389144537224,-23.6118258947772));
#58019=CARTESIAN_POINT('Ctrl Pts',(-27.1946650365021,25.0334415013223,-23.6060574257927));
#58020=CARTESIAN_POINT('Ctrl Pts',(-27.2347116519353,24.9262067428771,-23.6002889568082));
#58021=CARTESIAN_POINT('Ctrl Pts',(-27.2758596720533,24.8160226998534,-23.5943618372437));
#58022=CARTESIAN_POINT('Ctrl Pts',(-27.3120651220472,24.7039789531522,-23.5884347176793));
#58023=CARTESIAN_POINT('Ctrl Pts',(-27.3431712727172,24.590568072286,-23.5825075981148));
#58024=CARTESIAN_POINT('Ctrl Pts',(-27.373455648871,24.4801533246521,-23.576737063525));
#58025=CARTESIAN_POINT('Ctrl Pts',(-27.3989067254962,24.3684432134283,-23.5709665289351));
#58026=CARTESIAN_POINT('Ctrl Pts',(-27.4194311967607,24.2559050366811,-23.5651959943452));
#58027=CARTESIAN_POINT('Ctrl Pts',(-27.4407910734182,24.1387862303738,-23.5591905822935));
#58028=CARTESIAN_POINT('Ctrl Pts',(-27.4568146917436,24.0207710190427,-23.5531851702417));
#58029=CARTESIAN_POINT('Ctrl Pts',(-27.4674563763962,23.9023931840644,-23.54717975819));
#58030=CARTESIAN_POINT('Ctrl Pts',(-27.4780980610489,23.7840153490861,-23.5411743461382));
#58031=CARTESIAN_POINT('Ctrl Pts',(-27.4833578310401,23.6652754085337,-23.5351689340865));
#58032=CARTESIAN_POINT('Ctrl Pts',(-27.4832509332757,23.5467066668166,-23.5291635220347));
#58033=CARTESIAN_POINT('',(-27.4886967943341,23.5521013327097,-22.2791635220347));
#58034=CARTESIAN_POINT('Ctrl Pts',(-27.4843392770373,23.5467056856009,-23.5291635220347));
#58035=CARTESIAN_POINT('Ctrl Pts',(-27.4868379542081,23.2776309960683,-23.5155389993243));
#58036=CARTESIAN_POINT('Ctrl Pts',(-27.3387877591575,21.7019972671522,-23.4356188394893));
#58037=CARTESIAN_POINT('Ctrl Pts',(-25.2134988325905,19.2057890924782,-23.2894030425282));
#58038=CARTESIAN_POINT('Ctrl Pts',(-20.7942376834532,19.8025688486209,-23.0905161311538));
#58039=CARTESIAN_POINT('Ctrl Pts',(-18.9075205083243,23.8431521583261,-22.8916292197787));
#58040=CARTESIAN_POINT('Ctrl Pts',(-21.2870804239101,27.6145855449523,-22.6927423084039));
#58041=CARTESIAN_POINT('Ctrl Pts',(-25.7463036211984,27.6512414910055,-22.4938553970289));
#58042=CARTESIAN_POINT('Ctrl Pts',(-27.4384619512156,25.064519459982,-22.3559958015726));
#58043=CARTESIAN_POINT('Ctrl Pts',(-27.48929941677,23.655847641776,-22.2844318432412));
#58044=CARTESIAN_POINT('Ctrl Pts',(-27.4886967943341,23.5521013327097,-22.2791635220347));
#58045=CARTESIAN_POINT('',(-27.4786334210255,23.5528998401325,-21.0291635220348));
#58046=CARTESIAN_POINT('Ctrl Pts',(-27.4886967943341,23.5521013327097,-22.2791635220347));
#58047=CARTESIAN_POINT('Ctrl Pts',(-27.4817161209215,22.3503221452475,-22.2181362061162));
#58048=CARTESIAN_POINT('Ctrl Pts',(-26.250718358874,19.8306521089372,-22.0908132530728));
#58049=CARTESIAN_POINT('Ctrl Pts',(-21.9586513526617,19.1790334203923,-21.8971946629042));
#58050=CARTESIAN_POINT('Ctrl Pts',(-19.0123446419315,22.5264640691018,-21.6983077515295));
#58051=CARTESIAN_POINT('Ctrl Pts',(-20.2359905307524,26.8146695119866,-21.4994208401545));
#58052=CARTESIAN_POINT('Ctrl Pts',(-24.5051621953605,28.1031525268998,-21.3005339287797));
#58053=CARTESIAN_POINT('Ctrl Pts',(-27.1783184065575,25.8212684194662,-21.1437814894064));
#58054=CARTESIAN_POINT('Ctrl Pts',(-27.4815824957208,24.0318261664217,-21.0533246871581));
#58055=CARTESIAN_POINT('Ctrl Pts',(-27.4786334210255,23.5528998401325,-21.0291635220348));
#58056=CARTESIAN_POINT('',(-27.4825165310185,23.5474017168375,-19.7791634816917));
#58057=CARTESIAN_POINT('Ctrl Pts',(-27.4786334210255,23.5528998401325,-21.0291635220348));
#58058=CARTESIAN_POINT('Ctrl Pts',(-27.4734905521056,22.717703864157,-20.9870290500331));
#58059=CARTESIAN_POINT('Ctrl Pts',(-26.8032339315992,20.5608468367781,-20.8785989409065));
#58060=CARTESIAN_POINT('Ctrl Pts',(-23.2513783123186,18.9079012919564,-20.7038731946549));
#58061=CARTESIAN_POINT('Ctrl Pts',(-19.4830103574363,21.2923127787233,-20.5049862832801));
#58062=CARTESIAN_POINT('Ctrl Pts',(-19.4520931154282,25.7515794567508,-20.3060993719051));
#58063=CARTESIAN_POINT('Ctrl Pts',(-23.18703691035,28.188013332395,-20.1072124605302));
#58064=CARTESIAN_POINT('Ctrl Pts',(-26.7802818937802,26.576037175659,-19.9315671772402));
#58065=CARTESIAN_POINT('Ctrl Pts',(-27.4733345361709,24.4006161878087,-19.822217531075));
#58066=CARTESIAN_POINT('Ctrl Pts',(-27.4790222659213,23.5474050497456,-19.7791635220348));
#58067=CARTESIAN_POINT('',(-27.4847537623865,23.5487013432092,-18.5291635220347));
#58068=CARTESIAN_POINT('Ctrl Pts',(-27.4832514979866,23.5474010158096,-19.7791634732061));
#58069=CARTESIAN_POINT('Ctrl Pts',(-27.4831548869444,23.4141486881421,-19.7724466029512));
#58070=CARTESIAN_POINT('Ctrl Pts',(-27.4762823074789,23.2811691169794,-19.7657297326962));
#58071=CARTESIAN_POINT('Ctrl Pts',(-27.4627405440319,23.1490960119743,-19.7590128624413));
#58072=CARTESIAN_POINT('Ctrl Pts',(-27.4491281784238,23.0163343226009,-19.7522609727033));
#58073=CARTESIAN_POINT('Ctrl Pts',(-27.4287770222172,22.8844887235092,-19.7455090829653));
#58074=CARTESIAN_POINT('Ctrl Pts',(-27.4018449061974,22.7541839538263,-19.7387571932273));
#58075=CARTESIAN_POINT('Ctrl Pts',(-27.3747435418534,22.6230603155519,-19.7319628728825));
#58076=CARTESIAN_POINT('Ctrl Pts',(-27.3409783391831,22.493497077691,-19.7251685525378));
#58077=CARTESIAN_POINT('Ctrl Pts',(-27.3007584029886,22.3661095042748,-19.7183742321931));
#58078=CARTESIAN_POINT('Ctrl Pts',(-27.2831265664499,22.3102646401587,-19.7153957007222));
#58079=CARTESIAN_POINT('Ctrl Pts',(-27.2642548609165,22.2548376114924,-19.7124171692514));
#58080=CARTESIAN_POINT('Ctrl Pts',(-27.2441637335036,22.1998788674267,-19.7094386377806));
#58081=CARTESIAN_POINT('Ctrl Pts',(-27.2045532517075,22.0915254491934,-19.7035663408119));
#58082=CARTESIAN_POINT('Ctrl Pts',(-27.1601048768239,21.9847348274173,-19.6976940438432));
#58083=CARTESIAN_POINT('Ctrl Pts',(-27.1109613358181,21.8799705757854,-19.6918217468745));
#58084=CARTESIAN_POINT('Ctrl Pts',(-27.0618814809385,21.7753420903032,-19.6859570599363));
#58085=CARTESIAN_POINT('Ctrl Pts',(-27.0081187338839,21.6727351235627,-19.6800923729981));
#58086=CARTESIAN_POINT('Ctrl Pts',(-26.9498649697813,21.5725962747063,-19.6742276860599));
#58087=CARTESIAN_POINT('Ctrl Pts',(-26.8916711160285,21.4725604123873,-19.668369030585));
#58088=CARTESIAN_POINT('Ctrl Pts',(-26.8289956387334,21.3749879743061,-19.6625103751102));
#58089=CARTESIAN_POINT('Ctrl Pts',(-26.7620774062967,21.2803031985846,-19.6566517196354));
#58090=CARTESIAN_POINT('Ctrl Pts',(-26.6925452887602,21.1819199521262,-19.6505642199175));
#58091=CARTESIAN_POINT('Ctrl Pts',(-26.6184324006713,21.0866549678212,-19.6444767201996));
#58092=CARTESIAN_POINT('Ctrl Pts',(-26.5400580247613,20.994953701102,-19.6383892204817));
#58093=CARTESIAN_POINT('Ctrl Pts',(-26.4647172958995,20.9068019271075,-19.6325373503983));
#58094=CARTESIAN_POINT('Ctrl Pts',(-26.3854391385356,20.8219434615173,-19.6266854803149));
#58095=CARTESIAN_POINT('Ctrl Pts',(-26.3025492523911,20.740741584707,-19.6208336102315));
#58096=CARTESIAN_POINT('Ctrl Pts',(-26.2196719869855,20.6595520716208,-19.6149826311485));
#58097=CARTESIAN_POINT('Ctrl Pts',(-26.1331843814294,20.5820183295237,-19.6091316520655));
#58098=CARTESIAN_POINT('Ctrl Pts',(-26.0434491507821,20.5084669346199,-19.6032806729825));
#58099=CARTESIAN_POINT('Ctrl Pts',(-25.953705852074,20.434908926738,-19.5974291678402));
#58100=CARTESIAN_POINT('Ctrl Pts',(-25.8607146675498,20.3653342398886,-19.5915776626979));
#58101=CARTESIAN_POINT('Ctrl Pts',(-25.7648709894502,20.3000288337671,-19.5857261575556));
#58102=CARTESIAN_POINT('Ctrl Pts',(-25.6689954837516,20.2347017411421,-19.5798727092559));
#58103=CARTESIAN_POINT('Ctrl Pts',(-25.5702659423666,20.1736469809691,-19.5740192609561));
#58104=CARTESIAN_POINT('Ctrl Pts',(-25.4691056757582,20.1171065092367,-19.5681658126563));
#58105=CARTESIAN_POINT('Ctrl Pts',(-25.3678303679599,20.0605017387103,-19.5623057077148));
#58106=CARTESIAN_POINT('Ctrl Pts',(-25.2641191786131,20.00842170519,-19.5564456027732));
#58107=CARTESIAN_POINT('Ctrl Pts',(-25.1584189795438,19.961061860246,-19.5505854978317));
#58108=CARTESIAN_POINT('Ctrl Pts',(-25.052647598006,19.9136701214106,-19.5447214464762));
#58109=CARTESIAN_POINT('Ctrl Pts',(-24.9448849230039,19.8710050524779,-19.5388573951208));
#58110=CARTESIAN_POINT('Ctrl Pts',(-24.8355950613967,19.8332129056829,-19.5329933437653));
#58111=CARTESIAN_POINT('Ctrl Pts',(-24.72614412835,19.7953650608077,-19.5271206499687));
#58112=CARTESIAN_POINT('Ctrl Pts',(-24.6151619113872,19.7624045886342,-19.5212479561722));
#58113=CARTESIAN_POINT('Ctrl Pts',(-24.5031249067341,19.7344271639807,-19.5153752623756));
#58114=CARTESIAN_POINT('Ctrl Pts',(-24.4724510490102,19.7267674131157,-19.5137674170523));
#58115=CARTESIAN_POINT('Ctrl Pts',(-24.4416981670942,19.7194808790896,-19.5121595717289));
#58116=CARTESIAN_POINT('Ctrl Pts',(-24.4108761116318,19.7125688483176,-19.5105517264056));
#58117=CARTESIAN_POINT('Ctrl Pts',(-24.2983054182734,19.6873241952645,-19.5046794294369));
#58118=CARTESIAN_POINT('Ctrl Pts',(-24.1844344454888,19.6669945005741,-19.4988071324682));
#58119=CARTESIAN_POINT('Ctrl Pts',(-24.0697303555742,19.6517102668859,-19.4929348354995));
#58120=CARTESIAN_POINT('Ctrl Pts',(-23.9551749130504,19.6364458403506,-19.4870701485613));
#58121=CARTESIAN_POINT('Ctrl Pts',(-23.8397889064191,19.626213926151,-19.4812054616231));
#58122=CARTESIAN_POINT('Ctrl Pts',(-23.7240517836723,19.6210945022925,-19.4753407746849));
#58123=CARTESIAN_POINT('Ctrl Pts',(-23.608433689311,19.615980343441,-19.4694821192101));
#58124=CARTESIAN_POINT('Ctrl Pts',(-23.4924656075789,19.6159682349018,-19.4636234637352));
#58125=CARTESIAN_POINT('Ctrl Pts',(-23.3766335756227,19.6210865313714,-19.4577648082604));
#58126=CARTESIAN_POINT('Ctrl Pts',(-23.2562770424747,19.6264047530092,-19.4516773085425));
#58127=CARTESIAN_POINT('Ctrl Pts',(-23.1360678549191,19.6372624066566,-19.4455898088246));
#58128=CARTESIAN_POINT('Ctrl Pts',(-23.0165533679367,19.6536316619399,-19.4395023091067));
#58129=CARTESIAN_POINT('Ctrl Pts',(-22.901664943573,19.6693673103537,-19.4336504390233));
#58130=CARTESIAN_POINT('Ctrl Pts',(-22.7874188878009,19.6901957562352,-19.4277985689399));
#58131=CARTESIAN_POINT('Ctrl Pts',(-22.6742968890025,19.7160393513876,-19.4219466988565));
#58132=CARTESIAN_POINT('Ctrl Pts',(-22.5611921140569,19.7418790116177,-19.4160957197736));
#58133=CARTESIAN_POINT('Ctrl Pts',(-22.4492114586774,19.7727322107903,-19.4102447406906));
#58134=CARTESIAN_POINT('Ctrl Pts',(-22.3388257397701,19.8084703189233,-19.4043937616076));
#58135=CARTESIAN_POINT('Ctrl Pts',(-22.2284300961243,19.8442116402562,-19.3985422564653));
#58136=CARTESIAN_POINT('Ctrl Pts',(-22.1196300673251,19.8848386163031,-19.392690751323));
#58137=CARTESIAN_POINT('Ctrl Pts',(-22.0128799623301,19.9301731702759,-19.3868392461807));
#58138=CARTESIAN_POINT('Ctrl Pts',(-21.9060944079491,19.9755227788672,-19.380985797881));
#58139=CARTESIAN_POINT('Ctrl Pts',(-21.8013605112626,20.0255829123746,-19.3751323495812));
#58140=CARTESIAN_POINT('Ctrl Pts',(-21.699110651154,20.0801282200722,-19.3692789012814));
#58141=CARTESIAN_POINT('Ctrl Pts',(-21.5967445107514,20.1347355576289,-19.3634187963399));
#58142=CARTESIAN_POINT('Ctrl Pts',(-21.4968684102677,20.1938380553713,-19.3575586913983));
#58143=CARTESIAN_POINT('Ctrl Pts',(-21.3998883395547,20.2571654023937,-19.3516985864568));
#58144=CARTESIAN_POINT('Ctrl Pts',(-21.3028429588338,20.3205353964209,-19.3458345351014));
#58145=CARTESIAN_POINT('Ctrl Pts',(-21.208697826273,20.3881356645102,-19.3399704837459));
#58146=CARTESIAN_POINT('Ctrl Pts',(-21.1178268557636,20.4596548013071,-19.3341064323905));
#58147=CARTESIAN_POINT('Ctrl Pts',(-21.0268219595834,20.531279343035,-19.3282337385939));
#58148=CARTESIAN_POINT('Ctrl Pts',(-20.9391011681863,20.6068340117496,-19.3223610447973));
#58149=CARTESIAN_POINT('Ctrl Pts',(-20.8550025408124,20.6859696394764,-19.3164883510008));
#58150=CARTESIAN_POINT('Ctrl Pts',(-20.8319777434356,20.7076356505707,-19.3148805056774));
#58151=CARTESIAN_POINT('Ctrl Pts',(-20.8092242237213,20.7295698855669,-19.3132726603541));
#58152=CARTESIAN_POINT('Ctrl Pts',(-20.7867483886439,20.7517647523133,-19.3116648150308));
#58153=CARTESIAN_POINT('Ctrl Pts',(-20.7046604064988,20.8328265602026,-19.3057925180621));
#58154=CARTESIAN_POINT('Ctrl Pts',(-20.626004605136,20.9176390583445,-19.2999202210933));
#58155=CARTESIAN_POINT('Ctrl Pts',(-20.551143299641,21.00587975747,-19.2940479241246));
#58156=CARTESIAN_POINT('Ctrl Pts',(-20.4763790084525,21.0940061036575,-19.2881832371864));
#58157=CARTESIAN_POINT('Ctrl Pts',(-20.4053996992186,21.1855515036248,-19.2823185502482));
#58158=CARTESIAN_POINT('Ctrl Pts',(-20.3385318207419,21.2801558212345,-19.27645386331));
#58159=CARTESIAN_POINT('Ctrl Pts',(-20.2717327116923,21.3746628442257,-19.2705952078352));
#58160=CARTESIAN_POINT('Ctrl Pts',(-20.209036860163,21.4722221919493,-19.2647365523604));
#58161=CARTESIAN_POINT('Ctrl Pts',(-20.1507308451182,21.5724402801143,-19.2588778968856));
#58162=CARTESIAN_POINT('Ctrl Pts',(-20.0901473457704,21.676572975074,-19.2527903971677));
#58163=CARTESIAN_POINT('Ctrl Pts',(-20.0343039100533,21.7835760035491,-19.2467028974498));
#58164=CARTESIAN_POINT('Ctrl Pts',(-19.9834729923779,21.8929738231136,-19.2406153977319));
#58165=CARTESIAN_POINT('Ctrl Pts',(-19.9346095935704,21.9981371672063,-19.2347635276485));
#58166=CARTESIAN_POINT('Ctrl Pts',(-19.8903780781764,22.1055129487554,-19.2289116575651));
#58167=CARTESIAN_POINT('Ctrl Pts',(-19.8509734924559,22.214653943101,-19.2230597874817));
#58168=CARTESIAN_POINT('Ctrl Pts',(-19.8115749064419,22.3237783197377,-19.2172088083987));
#58169=CARTESIAN_POINT('Ctrl Pts',(-19.7770019291389,22.4346669860602,-19.2113578293158));
#58170=CARTESIAN_POINT('Ctrl Pts',(-19.7474008384818,22.5468543059475,-19.2055068502328));
#58171=CARTESIAN_POINT('Ctrl Pts',(-19.7177970864018,22.6590517125545,-19.1996553450905));
#58172=CARTESIAN_POINT('Ctrl Pts',(-19.6931662150729,22.7725476051101,-19.1938038399482));
#58173=CARTESIAN_POINT('Ctrl Pts',(-19.6736039787566,22.8868635078125,-19.1879523348059));
#58174=CARTESIAN_POINT('Ctrl Pts',(-19.6540352462474,23.0012173723376,-19.1820988865061));
#58175=CARTESIAN_POINT('Ctrl Pts',(-19.6395385653444,23.1163913812315,-19.1762454382064));
#58176=CARTESIAN_POINT('Ctrl Pts',(-19.6301580638171,23.2318999552646,-19.1703919899066));
#58177=CARTESIAN_POINT('Ctrl Pts',(-19.6207668946226,23.3475398876284,-19.164531884965));
#58178=CARTESIAN_POINT('Ctrl Pts',(-19.6165035512497,23.4635147322737,-19.1586717800235));
#58179=CARTESIAN_POINT('Ctrl Pts',(-19.6173600713241,23.5793368086224,-19.152811675082));
#58180=CARTESIAN_POINT('Ctrl Pts',(-19.6182171682113,23.6952368838906,-19.1469476237265));
#58181=CARTESIAN_POINT('Ctrl Pts',(-19.6242009727242,23.8109835741852,-19.1410835723711));
#58182=CARTESIAN_POINT('Ctrl Pts',(-19.6352516106229,23.9260939716803,-19.1352195210156));
#58183=CARTESIAN_POINT('Ctrl Pts',(-19.646318534956,24.0413740189231,-19.1293468272191));
#58184=CARTESIAN_POINT('Ctrl Pts',(-19.662467138922,24.1560154939564,-19.1234741334225));
#58185=CARTESIAN_POINT('Ctrl Pts',(-19.6835863969961,24.2695452417774,-19.1176014396259));
#58186=CARTESIAN_POINT('Ctrl Pts',(-19.6893684965749,24.3006277876107,-19.1159935943026));
#58187=CARTESIAN_POINT('Ctrl Pts',(-19.6955228944996,24.3316270893847,-19.1143857489792));
#58188=CARTESIAN_POINT('Ctrl Pts',(-19.7020466666069,24.3625336529246,-19.1127779036558));
#58189=CARTESIAN_POINT('Ctrl Pts',(-19.7258732913532,24.475412993214,-19.1069056066871));
#58190=CARTESIAN_POINT('Ctrl Pts',(-19.7547106739523,24.5874321893099,-19.1010333097184));
#58191=CARTESIAN_POINT('Ctrl Pts',(-19.7884833454349,24.6981121003305,-19.0951610127497));
#58192=CARTESIAN_POINT('Ctrl Pts',(-19.8222122502174,24.8086485789765,-19.0892963258115));
#58193=CARTESIAN_POINT('Ctrl Pts',(-19.8608636055139,24.9178488323108,-19.0834316388733));
#58194=CARTESIAN_POINT('Ctrl Pts',(-19.9043108821663,25.0252435446287,-19.0775669519351));
#58195=CARTESIAN_POINT('Ctrl Pts',(-19.9477134760145,25.1325278082081,-19.0717082964603));
#58196=CARTESIAN_POINT('Ctrl Pts',(-19.9959020265119,25.2380098433052,-19.0658496409854));
#58197=CARTESIAN_POINT('Ctrl Pts',(-20.0487003126699,25.3412357972347,-19.0599909855106));
#58198=CARTESIAN_POINT('Ctrl Pts',(-20.1035609463894,25.4484938478449,-19.0539034857927));
#58199=CARTESIAN_POINT('Ctrl Pts',(-20.1633986451923,25.5533155403398,-19.0478159860748));
#58200=CARTESIAN_POINT('Ctrl Pts',(-20.2279606004165,25.6552146034111,-19.0417284863569));
#58201=CARTESIAN_POINT('Ctrl Pts',(-20.2900235477364,25.7531694463428,-19.0358766162735));
#58202=CARTESIAN_POINT('Ctrl Pts',(-20.3564515851535,25.8484233242809,-19.0300247461901));
#58203=CARTESIAN_POINT('Ctrl Pts',(-20.4269738858302,25.9405703976464,-19.0241728761067));
#58204=CARTESIAN_POINT('Ctrl Pts',(-20.4974854488454,26.0327034407821,-19.0183218970237));
#58205=CARTESIAN_POINT('Ctrl Pts',(-20.5720897844552,26.1217302917127,-19.0124709179407));
#58206=CARTESIAN_POINT('Ctrl Pts',(-20.6504742146036,26.2072761882941,-19.0066199388578));
#58207=CARTESIAN_POINT('Ctrl Pts',(-20.7288656922667,26.2928297762749,-19.0007684337155));
#58208=CARTESIAN_POINT('Ctrl Pts',(-20.8110376608059,26.3749014829454,-18.9949169285732));
#58209=CARTESIAN_POINT('Ctrl Pts',(-20.8966393297389,26.4531521121841,-18.9890654234309));
#58210=CARTESIAN_POINT('Ctrl Pts',(-20.9822694251227,26.5314287267534,-18.9832119751311));
#58211=CARTESIAN_POINT('Ctrl Pts',(-21.0713311806373,26.605881462006,-18.9773585268313));
#58212=CARTESIAN_POINT('Ctrl Pts',(-21.1634399232597,26.6762107163502,-18.9715050785316));
#58213=CARTESIAN_POINT('Ctrl Pts',(-21.2556534135233,26.7466199503283,-18.96564497359));
#58214=CARTESIAN_POINT('Ctrl Pts',(-21.3509204783491,26.8128960926927,-18.9597848686485));
#58215=CARTESIAN_POINT('Ctrl Pts',(-21.4488265198836,26.874782230296,-18.9539247637069));
#58216=CARTESIAN_POINT('Ctrl Pts',(-21.5467984950092,26.9367100443397,-18.9480607123515));
#58217=CARTESIAN_POINT('Ctrl Pts',(-21.6474126275914,26.9942417621599,-18.942196660996));
#58218=CARTESIAN_POINT('Ctrl Pts',(-21.7502302746088,27.0471667248075,-18.9363326096406));
#58219=CARTESIAN_POINT('Ctrl Pts',(-21.8531994543136,27.1001696882853,-18.930459915844));
#58220=CARTESIAN_POINT('Ctrl Pts',(-21.9583782557738,27.148552174076,-18.9245872220475));
#58221=CARTESIAN_POINT('Ctrl Pts',(-22.0653085917438,27.1921518294789,-18.9187145282509));
#58222=CARTESIAN_POINT('Ctrl Pts',(-22.094584329006,27.2040886857949,-18.9171066829276));
#58223=CARTESIAN_POINT('Ctrl Pts',(-22.1239912746833,27.215667324323,-18.9154988376043));
#58224=CARTESIAN_POINT('Ctrl Pts',(-22.1535198605328,27.2268850732069,-18.9138909922809));
#58225=CARTESIAN_POINT('Ctrl Pts',(-22.2613664441935,27.2678554027602,-18.9080186953122));
#58226=CARTESIAN_POINT('Ctrl Pts',(-22.371197901153,27.3041451532595,-18.9021463983435));
#58227=CARTESIAN_POINT('Ctrl Pts',(-22.4825703279712,27.3355588220561,-18.8962741013748));
#58228=CARTESIAN_POINT('Ctrl Pts',(-22.5937984249692,27.3669317812327,-18.8904094144366));
#58229=CARTESIAN_POINT('Ctrl Pts',(-22.7065631263732,27.3934411137744,-18.8845447274984));
#58230=CARTESIAN_POINT('Ctrl Pts',(-22.8204011946328,27.4149395857504,-18.8786800405602));
#58231=CARTESIAN_POINT('Ctrl Pts',(-22.9341221875655,27.4364159478938,-18.8728213850854));
#58232=CARTESIAN_POINT('Ctrl Pts',(-23.0489139478978,27.4528916235118,-18.8669627296105));
#58233=CARTESIAN_POINT('Ctrl Pts',(-23.1642993868358,27.4642695436621,-18.8611040741357));
#58234=CARTESIAN_POINT('Ctrl Pts',(-23.284191882649,27.476091895395,-18.8550165744178));
#58235=CARTESIAN_POINT('Ctrl Pts',(-23.4047249441723,27.4824100039208,-18.8489290746999));
#58236=CARTESIAN_POINT('Ctrl Pts',(-23.5253528093961,27.4831737111522,-18.842841574982));
#58237=CARTESIAN_POINT('Ctrl Pts',(-23.6413115163265,27.4839078574696,-18.8369897048986));
#58238=CARTESIAN_POINT('Ctrl Pts',(-23.7573573723373,27.4795095941686,-18.8311378348152));
#58239=CARTESIAN_POINT('Ctrl Pts',(-23.8730025443944,27.4699873989144,-18.8252859647318));
#58240=CARTESIAN_POINT('Ctrl Pts',(-23.9886301084224,27.4604666535011,-18.8194349856488));
#58241=CARTESIAN_POINT('Ctrl Pts',(-24.1038566979243,27.4458235612667,-18.8135840065658));
#58242=CARTESIAN_POINT('Ctrl Pts',(-24.2181980034755,27.4261186086797,-18.8077330274829));
#58243=CARTESIAN_POINT('Ctrl Pts',(-24.3325495894105,27.4064118844278,-18.8018815223406));
#58244=CARTESIAN_POINT('Ctrl Pts',(-24.4460153257643,27.3816424653162,-18.7960300171983));
#58245=CARTESIAN_POINT('Ctrl Pts',(-24.5581202240218,27.35192212738,-18.790178512056));
#58246=CARTESIAN_POINT('Ctrl Pts',(-24.6702623498755,27.3221919199667,-18.7843250637562));
#58247=CARTESIAN_POINT('Ctrl Pts',(-24.7810423396812,27.2875076304317,-18.7784716154564));
#58248=CARTESIAN_POINT('Ctrl Pts',(-24.8900002015165,27.2480309432821,-18.7726181671567));
#58249=CARTESIAN_POINT('Ctrl Pts',(-24.9990819721007,27.208509362567,-18.7667580622151));
#58250=CARTESIAN_POINT('Ctrl Pts',(-25.1063370898653,27.1641846471078,-18.7608979572736));
#58251=CARTESIAN_POINT('Ctrl Pts',(-25.211325301753,27.1152667325873,-18.755037852332));
#58252=CARTESIAN_POINT('Ctrl Pts',(-25.3163842166304,27.066315874913,-18.7491738009766));
#58253=CARTESIAN_POINT('Ctrl Pts',(-25.4191728201105,27.0127658494672,-18.7433097496211));
#58254=CARTESIAN_POINT('Ctrl Pts',(-25.5192767761365,26.954871823891,-18.7374456982657));
#58255=CARTESIAN_POINT('Ctrl Pts',(-25.619528265411,26.8968924740778,-18.7315730044691));
#58256=CARTESIAN_POINT('Ctrl Pts',(-25.7170868635152,26.8345565683424,-18.7257003106725));
#58257=CARTESIAN_POINT('Ctrl Pts',(-25.8115683648219,26.7681617446531,-18.7198276168759));
#58258=CARTESIAN_POINT('Ctrl Pts',(-25.837435819397,26.7499839525769,-18.7182197715526));
#58259=CARTESIAN_POINT('Ctrl Pts',(-25.8630728230474,26.7315021407593,-18.7166119262293));
#58260=CARTESIAN_POINT('Ctrl Pts',(-25.8884719558549,26.7127229148721,-18.715004080906));
#58261=CARTESIAN_POINT('Ctrl Pts',(-25.9803593868226,26.6447845787322,-18.709187316323));
#58262=CARTESIAN_POINT('Ctrl Pts',(-26.0694515345047,26.5727136196195,-18.7033705517401));
#58263=CARTESIAN_POINT('Ctrl Pts',(-26.155348143687,26.4967701122248,-18.6975537871571));
#58264=CARTESIAN_POINT('Ctrl Pts',(-26.2411330667938,26.4209253494997,-18.6917445857552));
#58265=CARTESIAN_POINT('Ctrl Pts',(-26.3237303977159,26.3412183244325,-18.6859353843533));
#58266=CARTESIAN_POINT('Ctrl Pts',(-26.4027696642176,26.2579517411081,-18.6801261829514));
#58267=CARTESIAN_POINT('Ctrl Pts',(-26.4817283079108,26.1747700926027,-18.6743229071375));
#58268=CARTESIAN_POINT('Ctrl Pts',(-26.557135814654,26.0880364092415,-18.6685196313236));
#58269=CARTESIAN_POINT('Ctrl Pts',(-26.6286561731011,25.9980923999398,-18.6627163555098));
#58270=CARTESIAN_POINT('Ctrl Pts',(-26.7001248679531,25.9082133627802,-18.6569172717623));
#58271=CARTESIAN_POINT('Ctrl Pts',(-26.7677117365892,25.815128940433,-18.6511181880149));
#58272=CARTESIAN_POINT('Ctrl Pts',(-26.8311194402516,25.7192157237131,-18.6453191042674));
#58273=CARTESIAN_POINT('Ctrl Pts',(-26.8945033838994,25.6233384474121,-18.6395221935416));
#58274=CARTESIAN_POINT('Ctrl Pts',(-26.9537110422492,25.524634834789,-18.6337252828158));
#58275=CARTESIAN_POINT('Ctrl Pts',(-27.0084874227957,25.4235118404842,-18.6279283720901));
#58276=CARTESIAN_POINT('Ctrl Pts',(-27.0632571596509,25.3224011111364,-18.6221321644572));
#58277=CARTESIAN_POINT('Ctrl Pts',(-27.1135964864597,25.2188719546065,-18.6163359568244));
#58278=CARTESIAN_POINT('Ctrl Pts',(-27.1592959605735,25.1133566640101,-18.6105397491915));
#58279=CARTESIAN_POINT('Ctrl Pts',(-27.2050014738847,25.0078274295408,-18.6047427755883));
#58280=CARTESIAN_POINT('Ctrl Pts',(-27.2460657490443,24.9003119269598,-18.5989458019851));
#58281=CARTESIAN_POINT('Ctrl Pts',(-27.2823274847592,24.7912624207381,-18.5931488283819));
#58282=CARTESIAN_POINT('Ctrl Pts',(-27.3186242467916,24.6821075802696,-18.5873462553049));
#58283=CARTESIAN_POINT('Ctrl Pts',(-27.3501090735423,24.5714161786179,-18.581543682228));
#58284=CARTESIAN_POINT('Ctrl Pts',(-27.3766705692112,24.4596556338248,-18.575741109151));
#58285=CARTESIAN_POINT('Ctrl Pts',(-27.4032457905336,24.3478373367671,-18.5699355375943));
#58286=CARTESIAN_POINT('Ctrl Pts',(-27.4248925360662,24.2349492107402,-18.5641299660375));
#58287=CARTESIAN_POINT('Ctrl Pts',(-27.4415509003059,24.1214670329453,-18.5583243944808));
#58288=CARTESIAN_POINT('Ctrl Pts',(-27.4582343676282,24.0078138448145,-18.5525100743014));
#58289=CARTESIAN_POINT('Ctrl Pts',(-27.4699143998778,23.8935652367043,-18.5466957541221));
#58290=CARTESIAN_POINT('Ctrl Pts',(-27.476583114686,23.7792004582255,-18.5408814339428));
#58291=CARTESIAN_POINT('Ctrl Pts',(-27.4810630544585,23.7023719636196,-18.5369754633068));
#58292=CARTESIAN_POINT('Ctrl Pts',(-27.4832825003658,23.6254910618527,-18.5330694926707));
#58293=CARTESIAN_POINT('Ctrl Pts',(-27.4832522260306,23.5487019351943,-18.5291635220347));
#58294=CARTESIAN_POINT('',(-27.4832508811685,23.5538557292739,-17.2791635220348));
#58295=CARTESIAN_POINT('Ctrl Pts',(-27.4890146679522,23.5486996633349,-18.5291635220347));
#58296=CARTESIAN_POINT('Ctrl Pts',(-27.4894437676505,23.4630796333703,-18.5248147378669));
#58297=CARTESIAN_POINT('Ctrl Pts',(-27.4868948921978,23.3774856217654,-18.520465953699));
#58298=CARTESIAN_POINT('Ctrl Pts',(-27.3957955962931,21.9903054538677,-18.4498215324062));
#58299=CARTESIAN_POINT('Ctrl Pts',(-25.8029561903201,19.480107932479,-18.3172302581562));
#58300=CARTESIAN_POINT('Ctrl Pts',(-21.3436534168568,19.454929445721,-18.1183433467813));
#58301=CARTESIAN_POINT('Ctrl Pts',(-18.9120281411762,23.1930056488349,-17.9194564354064));
#58302=CARTESIAN_POINT('Ctrl Pts',(-20.7425378238047,27.2593614477559,-17.7205695240317));
#58303=CARTESIAN_POINT('Ctrl Pts',(-25.1530992680317,27.9173606333916,-17.5216826126568));
#58304=CARTESIAN_POINT('Ctrl Pts',(-27.3263780446851,25.4353497891762,-17.3745472786577));
#58305=CARTESIAN_POINT('Ctrl Pts',(-27.4864548523518,23.841195331127,-17.2937075817838));
#58306=CARTESIAN_POINT('Ctrl Pts',(-27.4837830291836,23.5538562167988,-17.2791635220348));
#58307=CARTESIAN_POINT('',(-27.4832525305424,23.550157346478,-16.029163521997));
#58308=CARTESIAN_POINT('Ctrl Pts',(-27.4832508811685,23.5538557292739,-17.2791635220348));
#58309=CARTESIAN_POINT('Ctrl Pts',(-27.4833554833984,23.4396792545031,-17.2733834885699));
#58310=CARTESIAN_POINT('Ctrl Pts',(-27.4784840087521,23.3253527973785,-17.267603455105));
#58311=CARTESIAN_POINT('Ctrl Pts',(-27.4686240491294,23.2113518805405,-17.2618234216402));
#58312=CARTESIAN_POINT('Ctrl Pts',(-27.4587719553128,23.0974419082031,-17.2560479992106));
#58313=CARTESIAN_POINT('Ctrl Pts',(-27.4439393254061,22.9838573821482,-17.2502725767811));
#58314=CARTESIAN_POINT('Ctrl Pts',(-27.4241658163455,22.8710729803218,-17.2444971543516));
#58315=CARTESIAN_POINT('Ctrl Pts',(-27.4044007235877,22.7583365835151,-17.2387241901456));
#58316=CARTESIAN_POINT('Ctrl Pts',(-27.3796990029499,22.6464000529191,-17.2329512259396));
#58317=CARTESIAN_POINT('Ctrl Pts',(-27.3501519843061,22.5357313884744,-17.2271782617335));
#58318=CARTESIAN_POINT('Ctrl Pts',(-27.3206099289805,22.4250813141896,-17.221406267272));
#58319=CARTESIAN_POINT('Ctrl Pts',(-27.2862243030079,22.3156990939649,-17.2156342728105));
#58320=CARTESIAN_POINT('Ctrl Pts',(-27.2471370162021,22.2080401385893,-17.2098622783489));
#58321=CARTESIAN_POINT('Ctrl Pts',(-27.2080462240232,22.1003715282889,-17.2040897662512));
#58322=CARTESIAN_POINT('Ctrl Pts',(-27.1642530792576,21.9944268897999,-17.1983172541535));
#58323=CARTESIAN_POINT('Ctrl Pts',(-27.1159482858359,21.8906433039252,-17.1925447420557));
#58324=CARTESIAN_POINT('Ctrl Pts',(-27.0675959483043,21.7867575688049,-17.186766548349));
#58325=CARTESIAN_POINT('Ctrl Pts',(-27.0147232731088,21.6850375211772,-17.1809883546422));
#58326=CARTESIAN_POINT('Ctrl Pts',(-26.9575677724546,21.5858972048549,-17.1752101609355));
#58327=CARTESIAN_POINT('Ctrl Pts',(-26.9003845973986,21.4867088852973,-17.1694291694568));
#58328=CARTESIAN_POINT('Ctrl Pts',(-26.8389146971259,21.3901031427884,-17.1636481779782));
#58329=CARTESIAN_POINT('Ctrl Pts',(-26.7734388437342,21.2964648314265,-17.1578671864995));
#58330=CARTESIAN_POINT('Ctrl Pts',(-26.7078547407901,21.2026717102413,-17.1520766374556));
#58331=CARTESIAN_POINT('Ctrl Pts',(-26.6382517134931,21.1118561586708,-17.1462860884118));
#58332=CARTESIAN_POINT('Ctrl Pts',(-26.5649509698691,21.0243700469246,-17.1404955393679));
#58333=CARTESIAN_POINT('Ctrl Pts',(-26.4949621506987,20.94083679266,-17.1349666228809));
#58334=CARTESIAN_POINT('Ctrl Pts',(-26.4216027264079,20.8603388731378,-17.129437706394));
#58335=CARTESIAN_POINT('Ctrl Pts',(-26.345181578633,20.7831492407819,-17.123908789907));
#58336=CARTESIAN_POINT('Ctrl Pts',(-26.2640141970163,20.7011656468592,-17.1180364929383));
#58337=CARTESIAN_POINT('Ctrl Pts',(-26.1791005452029,20.6226190577235,-17.1121641959696));
#58338=CARTESIAN_POINT('Ctrl Pts',(-26.0907635784659,20.5478713731418,-17.1062918990009));
#58339=CARTESIAN_POINT('Ctrl Pts',(-26.0025410894224,20.473220555623,-17.1004272120627));
#58340=CARTESIAN_POINT('Ctrl Pts',(-25.9109044204077,20.4023591169809,-17.0945625251245));
#58341=CARTESIAN_POINT('Ctrl Pts',(-25.8162141273757,20.3356130422808,-17.0886978381862));
#58342=CARTESIAN_POINT('Ctrl Pts',(-25.7216212173822,20.26893561174,-17.0828391827114));
#58343=CARTESIAN_POINT('Ctrl Pts',(-25.6239812657574,20.2063653634263,-17.0769805272366));
#58344=CARTESIAN_POINT('Ctrl Pts',(-25.5236882252713,20.1481883695544,-17.0711218717617));
#58345=CARTESIAN_POINT('Ctrl Pts',(-25.4194776502871,20.0877389310604,-17.0650343720438));
#58346=CARTESIAN_POINT('Ctrl Pts',(-25.3124028442579,20.0320332461679,-17.0589468723259));
#58347=CARTESIAN_POINT('Ctrl Pts',(-25.2029396998435,19.9813431570764,-17.052859372608));
#58348=CARTESIAN_POINT('Ctrl Pts',(-25.0977135594381,19.9326151357826,-17.0470075025246));
#58349=CARTESIAN_POINT('Ctrl Pts',(-24.9902809442824,19.8885218413018,-17.0411556324412));
#58350=CARTESIAN_POINT('Ctrl Pts',(-24.8810893296753,19.8492577441892,-17.0353037623578));
#58351=CARTESIAN_POINT('Ctrl Pts',(-24.7719143404843,19.8099996253923,-17.0294527832748));
#58352=CARTESIAN_POINT('Ctrl Pts',(-24.660981273252,19.7755693818141,-17.0236018041918));
#58353=CARTESIAN_POINT('Ctrl Pts',(-24.548755951962,19.7461126920309,-17.0177508251089));
#58354=CARTESIAN_POINT('Ctrl Pts',(-24.4365205405355,19.7166533538078,-17.0118993199666));
#58355=CARTESIAN_POINT('Ctrl Pts',(-24.3229930439467,19.6921685632684,-17.0060478148242));
#58356=CARTESIAN_POINT('Ctrl Pts',(-24.2086520608296,19.6727534588337,-17.0001963096819));
#58357=CARTESIAN_POINT('Ctrl Pts',(-24.0942731075614,19.6533319070655,-16.9943428613822));
#58358=CARTESIAN_POINT('Ctrl Pts',(-23.9790805379398,19.6389834581653,-16.9884894130824));
#58359=CARTESIAN_POINT('Ctrl Pts',(-23.8635599875814,19.6297516149636,-16.9826359647826));
#58360=CARTESIAN_POINT('Ctrl Pts',(-23.7479080652722,19.6205092731515,-16.9767758598411));
#58361=CARTESIAN_POINT('Ctrl Pts',(-23.6319278300723,19.6163951839207,-16.9709157548996));
#58362=CARTESIAN_POINT('Ctrl Pts',(-23.5161069519088,19.6174007572968,-16.965055649958));
#58363=CARTESIAN_POINT('Ctrl Pts',(-23.4002080756329,19.6184070078635,-16.9591915986026));
#58364=CARTESIAN_POINT('Ctrl Pts',(-23.2844691818779,19.6245397644162,-16.9533275472471));
#58365=CARTESIAN_POINT('Ctrl Pts',(-23.1693731010162,19.6357385312995,-16.9474634958917));
#58366=CARTESIAN_POINT('Ctrl Pts',(-23.0541073915066,19.6469538029297,-16.9415908020951));
#58367=CARTESIAN_POINT('Ctrl Pts',(-22.9394867934044,19.663249928192,-16.9357181082986));
#58368=CARTESIAN_POINT('Ctrl Pts',(-22.8259843184395,19.6845152727397,-16.929845414502));
#58369=CARTESIAN_POINT('Ctrl Pts',(-22.7949092394588,19.6903373683511,-16.9282375691787));
#58370=CARTESIAN_POINT('Ctrl Pts',(-22.7639178835875,19.6965316548715,-16.9266297238553));
#58371=CARTESIAN_POINT('Ctrl Pts',(-22.7330197412293,19.7030951959216,-16.925021878532));
#58372=CARTESIAN_POINT('Ctrl Pts',(-22.6201711574278,19.7270670678756,-16.9191495815633));
#58373=CARTESIAN_POINT('Ctrl Pts',(-22.5081891655635,19.7560485865944,-16.9132772845946));
#58374=CARTESIAN_POINT('Ctrl Pts',(-22.3975528089986,19.789963666554,-16.9074049876259));
#58375=CARTESIAN_POINT('Ctrl Pts',(-22.2870598283654,19.8238347952634,-16.9015403006877));
#58376=CARTESIAN_POINT('Ctrl Pts',(-22.1779094067485,19.8626266507924,-16.8956756137495));
#58377=CARTESIAN_POINT('Ctrl Pts',(-22.0705706966308,19.9062121001151,-16.8898109268113));
#58378=CARTESIAN_POINT('Ctrl Pts',(-21.9633423776573,19.9497527245315,-16.8839522713365));
#58379=CARTESIAN_POINT('Ctrl Pts',(-21.8579224448277,19.9980769823059,-16.8780936158617));
#58380=CARTESIAN_POINT('Ctrl Pts',(-21.7547645236691,20.0510080685224,-16.8722349603868));
#58381=CARTESIAN_POINT('Ctrl Pts',(-21.6475771632496,20.1060066895878,-16.8661474606689));
#58382=CARTESIAN_POINT('Ctrl Pts',(-21.5428325640239,20.1659792362117,-16.860059960951));
#58383=CARTESIAN_POINT('Ctrl Pts',(-21.4410166715523,20.2306722741479,-16.8539724612331));
#58384=CARTESIAN_POINT('Ctrl Pts',(-21.3431417799254,20.2928612303443,-16.8481205911497));
#58385=CARTESIAN_POINT('Ctrl Pts',(-21.2479734685871,20.3594117970913,-16.8422687210663));
#58386=CARTESIAN_POINT('Ctrl Pts',(-21.1559172282474,20.4300526254914,-16.8364168509829));
#58387=CARTESIAN_POINT('Ctrl Pts',(-21.0638750043073,20.500682698183,-16.8305658719));
#58388=CARTESIAN_POINT('Ctrl Pts',(-20.9749442370804,20.5754015426521,-16.824714892817));
#58389=CARTESIAN_POINT('Ctrl Pts',(-20.889499286008,20.6538959988119,-16.818863913734));
#58390=CARTESIAN_POINT('Ctrl Pts',(-20.8040466526123,20.7323975123785,-16.8130124085918));
#58391=CARTESIAN_POINT('Ctrl Pts',(-20.7220807628415,20.8146750327801,-16.8071609034495));
#58392=CARTESIAN_POINT('Ctrl Pts',(-20.6439403610962,20.9003773333058,-16.8013093983072));
#58393=CARTESIAN_POINT('Ctrl Pts',(-20.5657740106245,20.9861080936998,-16.7954559500074));
#58394=CARTESIAN_POINT('Ctrl Pts',(-20.4914359525828,21.0752655903474,-16.7896025017077));
#58395=CARTESIAN_POINT('Ctrl Pts',(-20.4212252932704,21.1674647649802,-16.7837490534079));
#58396=CARTESIAN_POINT('Ctrl Pts',(-20.3509347891924,21.2597687900952,-16.7778889484664));
#58397=CARTESIAN_POINT('Ctrl Pts',(-20.2847813030186,21.355121068276,-16.7720288435248));
#58398=CARTESIAN_POINT('Ctrl Pts',(-20.2230212141286,21.4531066713853,-16.7661687385833));
#58399=CARTESIAN_POINT('Ctrl Pts',(-20.1612195336844,21.5511582616652,-16.7603046872278));
#58400=CARTESIAN_POINT('Ctrl Pts',(-20.1038173460744,21.6518463497796,-16.7544406358724));
#58401=CARTESIAN_POINT('Ctrl Pts',(-20.0510247455741,21.7547320219687,-16.748576584517));
#58402=CARTESIAN_POINT('Ctrl Pts',(-19.9981543393189,21.8577693271009,-16.7427038907204));
#58403=CARTESIAN_POINT('Ctrl Pts',(-19.9499072505361,21.963010305963,-16.7368311969239));
#58404=CARTESIAN_POINT('Ctrl Pts',(-19.9064452422692,22.0699966627535,-16.7309585031273));
#58405=CARTESIAN_POINT('Ctrl Pts',(-19.894546071436,22.0992877375805,-16.7293506578039));
#58406=CARTESIAN_POINT('Ctrl Pts',(-19.8830052869491,22.1287095597155,-16.7277428124805));
#58407=CARTESIAN_POINT('Ctrl Pts',(-19.871825548349,22.158252557485,-16.7261349671571));
#58408=CARTESIAN_POINT('Ctrl Pts',(-19.8309940428943,22.2661517774694,-16.7202626701884));
#58409=CARTESIAN_POINT('Ctrl Pts',(-19.7948456669953,22.3760298455675,-16.7143903732197));
#58410=CARTESIAN_POINT('Ctrl Pts',(-19.7635753518695,22.4874426071099,-16.708518076251));
#58411=CARTESIAN_POINT('Ctrl Pts',(-19.7323455605886,22.5987109865619,-16.7026533893128));
#58412=CARTESIAN_POINT('Ctrl Pts',(-19.7059813694057,22.7115097100381,-16.6967887023746));
#58413=CARTESIAN_POINT('Ctrl Pts',(-19.6846294159788,22.8253753508929,-16.6909240154364));
#58414=CARTESIAN_POINT('Ctrl Pts',(-19.6632994216993,22.9391238880638,-16.6850653599616));
#58415=CARTESIAN_POINT('Ctrl Pts',(-19.6469714877987,23.0539367562528,-16.6792067044868));
#58416=CARTESIAN_POINT('Ctrl Pts',(-19.6357420691627,23.1693367421408,-16.6733480490119));
#58417=CARTESIAN_POINT('Ctrl Pts',(-19.6240740195439,23.2892443531206,-16.667260549294));
#58418=CARTESIAN_POINT('Ctrl Pts',(-19.6179110329326,23.409785445747,-16.6611730495761));
#58419=CARTESIAN_POINT('Ctrl Pts',(-19.6173025650211,23.5304141939125,-16.6550855498582));
#58420=CARTESIAN_POINT('Ctrl Pts',(-19.6167176491553,23.6463737496085,-16.6492336797748));
#58421=CARTESIAN_POINT('Ctrl Pts',(-19.621265250812,23.7624138493004,-16.6433818096914));
#58422=CARTESIAN_POINT('Ctrl Pts',(-19.6309362645296,23.8780466712681,-16.637529939608));
#58423=CARTESIAN_POINT('Ctrl Pts',(-19.6406058057474,23.9936618870872,-16.6316789605251));
#58424=CARTESIAN_POINT('Ctrl Pts',(-19.6553971735216,24.1088695366498,-16.6258279814421));
#58425=CARTESIAN_POINT('Ctrl Pts',(-19.675249258165,24.2231853887741,-16.6199770023591));
#58426=CARTESIAN_POINT('Ctrl Pts',(-19.6951031277018,24.3375115189934,-16.6141254972168));
#58427=CARTESIAN_POINT('Ctrl Pts',(-19.7200185478864,24.4509452850703,-16.6082739920746));
#58428=CARTESIAN_POINT('Ctrl Pts',(-19.7498831315029,24.56301184273,-16.6024224869323));
#58429=CARTESIAN_POINT('Ctrl Pts',(-19.7797576324976,24.6751156152542,-16.5965690386325));
#58430=CARTESIAN_POINT('Ctrl Pts',(-19.8145844585482,24.7858508773396,-16.5907155903327));
#58431=CARTESIAN_POINT('Ctrl Pts',(-19.8542013333078,24.8947578455203,-16.584862142033));
#58432=CARTESIAN_POINT('Ctrl Pts',(-19.8938632610568,25.0037886645727,-16.5790020370914));
#58433=CARTESIAN_POINT('Ctrl Pts',(-19.9383259688121,25.110986651057,-16.5731419321499));
#58434=CARTESIAN_POINT('Ctrl Pts',(-19.9873789544936,25.2159118224514,-16.5672818272084));
#58435=CARTESIAN_POINT('Ctrl Pts',(-20.0364649742909,25.3209076543818,-16.5614177758529));
#58436=CARTESIAN_POINT('Ctrl Pts',(-20.0901472363368,25.4236272580234,-16.5555537244974));
#58437=CARTESIAN_POINT('Ctrl Pts',(-20.1481700399834,25.5236566260435,-16.549689673142));
#58438=CARTESIAN_POINT('Ctrl Pts',(-20.20627835766,25.6238334173842,-16.5438169793454));
#58439=CARTESIAN_POINT('Ctrl Pts',(-20.2687397621095,25.7213117132355,-16.5379442855488));
#58440=CARTESIAN_POINT('Ctrl Pts',(-20.3352561211675,25.8157076913255,-16.5320715917523));
#58441=CARTESIAN_POINT('Ctrl Pts',(-20.3534671875948,25.8415517310749,-16.5304637464289));
#58442=CARTESIAN_POINT('Ctrl Pts',(-20.3719819769394,25.8671649288407,-16.5288559011056));
#58443=CARTESIAN_POINT('Ctrl Pts',(-20.3907938739861,25.8925398732117,-16.5272480557822));
#58444=CARTESIAN_POINT('Ctrl Pts',(-20.4595001384502,25.9852162064063,-16.5213757588135));
#58445=CARTESIAN_POINT('Ctrl Pts',(-20.5324026710907,26.0750221954256,-16.5155034618448));
#58446=CARTESIAN_POINT('Ctrl Pts',(-20.6092331657192,26.161553756938,-16.5096311648761));
#58447=CARTESIAN_POINT('Ctrl Pts',(-20.6859640941281,26.2479731804187,-16.5037664779379));
#58448=CARTESIAN_POINT('Ctrl Pts',(-20.7666125897615,26.3311263087217,-16.4979017909997));
#58449=CARTESIAN_POINT('Ctrl Pts',(-20.8508680278774,26.4106392713771,-16.4920371040615));
#58450=CARTESIAN_POINT('Ctrl Pts',(-20.9350368145494,26.4900704599277,-16.4861784485867));
#58451=CARTESIAN_POINT('Ctrl Pts',(-21.0228048664517,26.5658686471914,-16.4803197931119));
#58452=CARTESIAN_POINT('Ctrl Pts',(-21.1138228339669,26.6376947300248,-16.4744611376371));
#58453=CARTESIAN_POINT('Ctrl Pts',(-21.2083960434611,26.7123264029175,-16.4683736379192));
#58454=CARTESIAN_POINT('Ctrl Pts',(-21.3064779316249,26.782668997622,-16.4622861382013));
#58455=CARTESIAN_POINT('Ctrl Pts',(-21.4076360186946,26.8483858640841,-16.4561986384834));
#58456=CARTESIAN_POINT('Ctrl Pts',(-21.504878566678,26.9115590193441,-16.4503467684));
#58457=CARTESIAN_POINT('Ctrl Pts',(-21.6049632209802,26.9704576389421,-16.4444948983166));
#58458=CARTESIAN_POINT('Ctrl Pts',(-21.7074746471155,27.0248256951357,-16.4386430282332));
#58459=CARTESIAN_POINT('Ctrl Pts',(-21.8099704649541,27.0791854732984,-16.4327920491502));
#58460=CARTESIAN_POINT('Ctrl Pts',(-21.9148919548463,27.1290158660044,-16.4269410700672));
#58461=CARTESIAN_POINT('Ctrl Pts',(-22.0217986925976,27.174106538377,-16.4210900909842));
#58462=CARTESIAN_POINT('Ctrl Pts',(-22.1287150422937,27.219201264835,-16.4152385858419));
#58463=CARTESIAN_POINT('Ctrl Pts',(-22.237616613764,27.25955526316,-16.4093870806996));
#58464=CARTESIAN_POINT('Ctrl Pts',(-22.3480431624985,27.295006413142,-16.4035355755573));
#58465=CARTESIAN_POINT('Ctrl Pts',(-22.4585063814865,27.3304693356792,-16.3976821272575));
#58466=CARTESIAN_POINT('Ctrl Pts',(-22.5704951913178,27.361026046148,-16.3918286789577));
#58467=CARTESIAN_POINT('Ctrl Pts',(-22.6835350512033,27.3865645379069,-16.3859752306578));
#58468=CARTESIAN_POINT('Ctrl Pts',(-22.796703461955,27.4121320724763,-16.3801151257163));
#58469=CARTESIAN_POINT('Ctrl Pts',(-22.9109249050284,27.4326699065753,-16.3742550207747));
#58470=CARTESIAN_POINT('Ctrl Pts',(-23.0257154304476,27.4481173099306,-16.3683949158332));
#58471=CARTESIAN_POINT('Ctrl Pts',(-23.1405832601013,27.4635751161453,-16.3625308644777));
#58472=CARTESIAN_POINT('Ctrl Pts',(-23.2560205244885,27.473935628753,-16.3566668131223));
#58473=CARTESIAN_POINT('Ctrl Pts',(-23.3715406952535,27.4791901844848,-16.3508027617668));
#58474=CARTESIAN_POINT('Ctrl Pts',(-23.4872311196903,27.4844524843829,-16.3449300679702));
#58475=CARTESIAN_POINT('Ctrl Pts',(-23.6030042825371,27.4845938081323,-16.3390573741736));
#58476=CARTESIAN_POINT('Ctrl Pts',(-23.718376114603,27.479657507116,-16.333184680377));
#58477=CARTESIAN_POINT('Ctrl Pts',(-23.7499629922859,27.4783060304721,-16.3315768350538));
#58478=CARTESIAN_POINT('Ctrl Pts',(-23.7815198338473,27.4765742467638,-16.3299689897305));
#58479=CARTESIAN_POINT('Ctrl Pts',(-23.8130368281386,27.4744637153007,-16.3283611444073));
#58480=CARTESIAN_POINT('Ctrl Pts',(-23.9281456308094,27.4667554691566,-16.3224888474386));
#58481=CARTESIAN_POINT('Ctrl Pts',(-24.0431078256081,27.4539652894805,-16.3166165504699));
#58482=CARTESIAN_POINT('Ctrl Pts',(-24.1574384195787,27.4361004825994,-16.3107442535012));
#58483=CARTESIAN_POINT('Ctrl Pts',(-24.271620850179,27.4182588270892,-16.304879566563));
#58484=CARTESIAN_POINT('Ctrl Pts',(-24.385172903006,27.3953556855317,-16.2990148796249));
#58485=CARTESIAN_POINT('Ctrl Pts',(-24.4976121287189,27.3674502988953,-16.2931501926867));
#58486=CARTESIAN_POINT('Ctrl Pts',(-24.6099357177269,27.3395736112022,-16.2872915372119));
#58487=CARTESIAN_POINT('Ctrl Pts',(-24.7211483572374,27.3067050100721,-16.2814328817371));
#58488=CARTESIAN_POINT('Ctrl Pts',(-24.8307759158083,27.268955109575,-16.2755742262623));
#58489=CARTESIAN_POINT('Ctrl Pts',(-24.9446856233762,27.2297306647146,-16.2694867265444));
#58490=CARTESIAN_POINT('Ctrl Pts',(-25.0568834470654,27.1852358810322,-16.2633992268265));
#58491=CARTESIAN_POINT('Ctrl Pts',(-25.1668523838908,27.1356526373837,-16.2573117271086));
#58492=CARTESIAN_POINT('Ctrl Pts',(-25.2725647389349,27.0879886187241,-16.2514598570252));
#58493=CARTESIAN_POINT('Ctrl Pts',(-25.376217134358,27.0356229205971,-16.2456079869418));
#58494=CARTESIAN_POINT('Ctrl Pts',(-25.4773696638282,26.9787665770257,-16.2397561168584));
#58495=CARTESIAN_POINT('Ctrl Pts',(-25.5785067919058,26.9219188903498,-16.2339051377754));
#58496=CARTESIAN_POINT('Ctrl Pts',(-25.67714445058,26.8605821202231,-16.2280541586925));
#58497=CARTESIAN_POINT('Ctrl Pts',(-25.772867613642,26.7950131079923,-16.2222031796095));
#58498=CARTESIAN_POINT('Ctrl Pts',(-25.8685993831377,26.7294382004762,-16.2163516744672));
#58499=CARTESIAN_POINT('Ctrl Pts',(-25.9614157950425,26.6596305280433,-16.210500169325));
#58500=CARTESIAN_POINT('Ctrl Pts',(-26.0509316732348,26.5858896692757,-16.2046486641827));
#58501=CARTESIAN_POINT('Ctrl Pts',(-26.1404772777018,26.5121243227739,-16.1987952158829));
#58502=CARTESIAN_POINT('Ctrl Pts',(-26.2267198501632,26.4344234554869,-16.1929417675831));
#58503=CARTESIAN_POINT('Ctrl Pts',(-26.3093086481386,26.3531257622044,-16.1870883192833));
#58504=CARTESIAN_POINT('Ctrl Pts',(-26.3919913675111,26.2717356157911,-16.1812282143418));
#58505=CARTESIAN_POINT('Ctrl Pts',(-26.4710117240994,26.1867407692892,-16.1753681094003));
#58506=CARTESIAN_POINT('Ctrl Pts',(-26.5460570290276,26.0985155506459,-16.1695080044587));
#58507=CARTESIAN_POINT('Ctrl Pts',(-26.6211528722716,26.0102309178398,-16.1636439531033));
#58508=CARTESIAN_POINT('Ctrl Pts',(-26.692268080494,25.9187119067542,-16.1577799017478));
#58509=CARTESIAN_POINT('Ctrl Pts',(-26.7591323759396,25.8243631589935,-16.1519158503924));
#58510=CARTESIAN_POINT('Ctrl Pts',(-26.8260952160093,25.7298753600124,-16.1460431565958));
#58511=CARTESIAN_POINT('Ctrl Pts',(-26.8887944165423,25.6325498471169,-16.1401704627993));
#58512=CARTESIAN_POINT('Ctrl Pts',(-26.9470047898657,25.5328173090992,-16.1342977690027));
#58513=CARTESIAN_POINT('Ctrl Pts',(-26.9629418163417,25.5055122085104,-16.1326899236793));
#58514=CARTESIAN_POINT('Ctrl Pts',(-26.9785426483065,25.4780268057239,-16.1310820783559));
#58515=CARTESIAN_POINT('Ctrl Pts',(-26.9938032942917,25.4503701978966,-16.1294742330325));
#58516=CARTESIAN_POINT('Ctrl Pts',(-27.0522995010747,25.3443585223778,-16.1233111353102));
#58517=CARTESIAN_POINT('Ctrl Pts',(-27.1059736427251,25.23550369087,-16.1171480375878));
#58518=CARTESIAN_POINT('Ctrl Pts',(-27.154553849024,25.1242604776381,-16.1109849398655));
#58519=CARTESIAN_POINT('Ctrl Pts',(-27.2030468990792,25.0132168424102,-16.1048328991659));
#58520=CARTESIAN_POINT('Ctrl Pts',(-27.2464640757081,24.8997936829022,-16.0986808584663));
#58521=CARTESIAN_POINT('Ctrl Pts',(-27.2845789882971,24.7844708736078,-16.0925288177667));
#58522=CARTESIAN_POINT('Ctrl Pts',(-27.3226063178148,24.6694130610072,-16.08639091365));
#58523=CARTESIAN_POINT('Ctrl Pts',(-27.3553555609326,24.552464635243,-16.0802530095332));
#58524=CARTESIAN_POINT('Ctrl Pts',(-27.3826484412697,24.4341250294386,-16.0741151054165));
#58525=CARTESIAN_POINT('Ctrl Pts',(-27.4099034846243,24.3159494815696,-16.0679857104702));
#58526=CARTESIAN_POINT('Ctrl Pts',(-27.4317171487945,24.1963869374792,-16.0618563155239));
#58527=CARTESIAN_POINT('Ctrl Pts',(-27.4479606124416,24.0759527478596,-16.0557269205776));
#58528=CARTESIAN_POINT('Ctrl Pts',(-27.4641760744772,23.955726171066,-16.0496080919083));
#58529=CARTESIAN_POINT('Ctrl Pts',(-27.4748404285476,23.8346312936653,-16.043489263239));
#58530=CARTESIAN_POINT('Ctrl Pts',(-27.4798758177641,23.7131937161043,-16.0373704345697));
#58531=CARTESIAN_POINT('Ctrl Pts',(-27.4821270655716,23.6589007769734,-16.034634797058));
#58532=CARTESIAN_POINT('Ctrl Pts',(-27.4832538466711,23.6045394782566,-16.0318991595464));
#58533=CARTESIAN_POINT('Ctrl Pts',(-27.4832525305424,23.5501573472289,-16.0291635220348));
#58534=CARTESIAN_POINT('',(-27.4832509111211,23.5466821780573,-14.7791635220348));
#58535=CARTESIAN_POINT('Ctrl Pts',(-27.4832525305424,23.5501573464781,-16.029163521997));
#58536=CARTESIAN_POINT('Ctrl Pts',(-27.4832495762865,23.4280891425663,-16.023023005778));
#58537=CARTESIAN_POINT('Ctrl Pts',(-27.4775593913889,23.3061351717897,-16.016882489559));
#58538=CARTESIAN_POINT('Ctrl Pts',(-27.4662395404907,23.1848284671646,-16.0107419733401));
#58539=CARTESIAN_POINT('Ctrl Pts',(-27.4549031186718,23.0633441838946,-16.0045924681328));
#58540=CARTESIAN_POINT('Ctrl Pts',(-27.4379206219041,22.9425094045615,-15.9984429629255));
#58541=CARTESIAN_POINT('Ctrl Pts',(-27.4154009443107,22.8228484153681,-15.9922934577182));
#58542=CARTESIAN_POINT('Ctrl Pts',(-27.3928252781756,22.70288992439,-15.9861286635785));
#58543=CARTESIAN_POINT('Ctrl Pts',(-27.3646849766341,22.5841114015368,-15.9799638694388));
#58544=CARTESIAN_POINT('Ctrl Pts',(-27.3311395629083,22.467024828394,-15.9737990752992));
#58545=CARTESIAN_POINT('Ctrl Pts',(-27.2975481124793,22.3497775692078,-15.9676258207839));
#58546=CARTESIAN_POINT('Ctrl Pts',(-27.2585368602675,22.2342272233437,-15.9614525662687));
#58547=CARTESIAN_POINT('Ctrl Pts',(-27.2143138399266,22.1208667441917,-15.9552793117535));
#58548=CARTESIAN_POINT('Ctrl Pts',(-27.1699909375302,22.0072502292108,-15.9490921143338));
#58549=CARTESIAN_POINT('Ctrl Pts',(-27.1204328800064,21.89583378649,-15.9429049169141));
#58550=CARTESIAN_POINT('Ctrl Pts',(-27.0658946150256,21.7870878366333,-15.9367177194943));
#58551=CARTESIAN_POINT('Ctrl Pts',(-27.0478820837194,21.7511719557942,-15.9346742535487));
#58552=CARTESIAN_POINT('Ctrl Pts',(-27.0293266648687,21.7155471448263,-15.9326307876031));
#58553=CARTESIAN_POINT('Ctrl Pts',(-27.010238574576,21.6802296486622,-15.9305873216575));
#58554=CARTESIAN_POINT('Ctrl Pts',(-26.9553852333662,21.5787379521096,-15.9247150246888));
#58555=CARTESIAN_POINT('Ctrl Pts',(-26.8959706312279,21.4794917935849,-15.9188427277201));
#58556=CARTESIAN_POINT('Ctrl Pts',(-26.8322029900957,21.3829292543315,-15.9129704307514));
#58557=CARTESIAN_POINT('Ctrl Pts',(-26.7685179867621,21.2864918524602,-15.9071057438132));
#58558=CARTESIAN_POINT('Ctrl Pts',(-26.7004913884387,21.1927314956184,-15.901241056875));
#58559=CARTESIAN_POINT('Ctrl Pts',(-26.6283775962247,21.1020623660598,-15.8953763699368));
#58560=CARTESIAN_POINT('Ctrl Pts',(-26.5563379685318,21.0114864840251,-15.8895177144619));
#58561=CARTESIAN_POINT('Ctrl Pts',(-26.480219763546,20.923995827398,-15.8836590589871));
#58562=CARTESIAN_POINT('Ctrl Pts',(-26.4003206508387,20.8399756609232,-15.8778004035123));
#58563=CARTESIAN_POINT('Ctrl Pts',(-26.3173006084149,20.7526735927419,-15.8717129037944));
#58564=CARTESIAN_POINT('Ctrl Pts',(-26.2301985161906,20.6691190420241,-15.8656254040765));
#58565=CARTESIAN_POINT('Ctrl Pts',(-26.1393946801444,20.5897066470441,-15.8595379043586));
#58566=CARTESIAN_POINT('Ctrl Pts',(-26.0521055998583,20.5133680778498,-15.8536860342752));
#58567=CARTESIAN_POINT('Ctrl Pts',(-25.9613963551964,20.4408572624481,-15.8478341641918));
#58568=CARTESIAN_POINT('Ctrl Pts',(-25.8676417262599,20.3724865993275,-15.8419822941084));
#58569=CARTESIAN_POINT('Ctrl Pts',(-25.7739013723181,20.3041263462621,-15.8361313150254));
#58570=CARTESIAN_POINT('Ctrl Pts',(-25.6771168899722,20.2399052355939,-15.8302803359425));
#58571=CARTESIAN_POINT('Ctrl Pts',(-25.5776943818048,20.1800939976754,-15.8244293568595));
#58572=CARTESIAN_POINT('Ctrl Pts',(-25.4782629345972,20.120277382151,-15.8185778517172));
#58573=CARTESIAN_POINT('Ctrl Pts',(-25.3761933443143,20.0648716406712,-15.8127263465749));
#58574=CARTESIAN_POINT('Ctrl Pts',(-25.2719181780131,20.0141025911112,-15.8068748414326));
#58575=CARTESIAN_POINT('Ctrl Pts',(-25.1676083841988,19.9633166822549,-15.8010213931328));
#58576=CARTESIAN_POINT('Ctrl Pts',(-25.0610919294624,19.9171707078654,-15.795167944833));
#58577=CARTESIAN_POINT('Ctrl Pts',(-24.9528226468318,19.8758429094388,-15.7893144965333));
#58578=CARTESIAN_POINT('Ctrl Pts',(-24.8444302385168,19.8344681123314,-15.7834543915917));
#58579=CARTESIAN_POINT('Ctrl Pts',(-24.7342814100818,19.7979225752351,-15.7775942866502));
#58580=CARTESIAN_POINT('Ctrl Pts',(-24.6228465880132,19.7663351184373,-15.7717341817086));
#58581=CARTESIAN_POINT('Ctrl Pts',(-24.5113367215664,19.7347263894643,-15.7658701303532));
#58582=CARTESIAN_POINT('Ctrl Pts',(-24.3985395383644,19.7080824841138,-15.7600060789977));
#58583=CARTESIAN_POINT('Ctrl Pts',(-24.2849354089757,19.6864810490843,-15.7541420276423));
#58584=CARTESIAN_POINT('Ctrl Pts',(-24.1711638497779,19.6648477778517,-15.7482693338457));
#58585=CARTESIAN_POINT('Ctrl Pts',(-24.0565833784125,19.6482718679334,-15.7423966400491));
#58586=CARTESIAN_POINT('Ctrl Pts',(-23.9416793155779,19.6367791290941,-15.7365239462526));
#58587=CARTESIAN_POINT('Ctrl Pts',(-23.9102205052853,19.6336326094501,-15.7349161009293));
#58588=CARTESIAN_POINT('Ctrl Pts',(-23.8787374356743,19.6308668090165,-15.733308255606));
#58589=CARTESIAN_POINT('Ctrl Pts',(-23.8472400398909,19.6284815771413,-15.7317004102828));
#58590=CARTESIAN_POINT('Ctrl Pts',(-23.7322028164066,19.6197700489188,-15.7258281133141));
#58591=CARTESIAN_POINT('Ctrl Pts',(-23.6165892468438,19.6161097945448,-15.7199558163454));
#58592=CARTESIAN_POINT('Ctrl Pts',(-23.5008804490858,19.6175624348955,-15.7140835193766));
#58593=CARTESIAN_POINT('Ctrl Pts',(-23.3853216007404,19.6190131927396,-15.7082188324384));
#58594=CARTESIAN_POINT('Ctrl Pts',(-23.2696681791491,19.6255636636195,-15.7023541455002));
#58595=CARTESIAN_POINT('Ctrl Pts',(-23.1544061573703,19.6372236986884,-15.696489458562));
#58596=CARTESIAN_POINT('Ctrl Pts',(-23.0392626753654,19.6488717421412,-15.6906308030872));
#58597=CARTESIAN_POINT('Ctrl Pts',(-22.9245102013308,19.6656188562266,-15.6847721476124));
#58598=CARTESIAN_POINT('Ctrl Pts',(-22.8106337679824,19.6874228584669,-15.6789134921376));
#58599=CARTESIAN_POINT('Ctrl Pts',(-22.6923092208463,19.7100785442394,-15.6728259924197));
#58600=CARTESIAN_POINT('Ctrl Pts',(-22.5749310020614,19.7381942190563,-15.6667384927018));
#58601=CARTESIAN_POINT('Ctrl Pts',(-22.459036698933,19.7716632438341,-15.6606509929839));
#58602=CARTESIAN_POINT('Ctrl Pts',(-22.3476283315013,19.8038367787653,-15.6547991229005));
#58603=CARTESIAN_POINT('Ctrl Pts',(-22.237591573722,19.8409568185651,-15.6489472528171));
#58604=CARTESIAN_POINT('Ctrl Pts',(-22.1293918362178,19.8828769190728,-15.6430953827337));
#58605=CARTESIAN_POINT('Ctrl Pts',(-22.0212085731075,19.924790636864,-15.6372444036507));
#58606=CARTESIAN_POINT('Ctrl Pts',(-21.9148621594914,19.9715028128932,-15.6313934245677));
#58607=CARTESIAN_POINT('Ctrl Pts',(-21.8107998810192,20.0228181274763,-15.6255424454848));
#58608=CARTESIAN_POINT('Ctrl Pts',(-21.7067282463467,20.0741380558001,-15.6196909403425));
#58609=CARTESIAN_POINT('Ctrl Pts',(-21.6049415258437,20.1300617625678,-15.6138394352002));
#58610=CARTESIAN_POINT('Ctrl Pts',(-21.5058635247093,20.1903473859915,-15.6079879300579));
#58611=CARTESIAN_POINT('Ctrl Pts',(-21.4067526219276,20.2506530289584,-15.6021344817581));
#58612=CARTESIAN_POINT('Ctrl Pts',(-21.3103525800872,20.3153232540631,-15.5962810334583));
#58613=CARTESIAN_POINT('Ctrl Pts',(-21.2170586727406,20.3840725910494,-15.5904275851586));
#58614=CARTESIAN_POINT('Ctrl Pts',(-21.123658669963,20.4529001109606,-15.584567480217));
#58615=CARTESIAN_POINT('Ctrl Pts',(-21.0333721851245,20.5258157563511,-15.5787073752755));
#58616=CARTESIAN_POINT('Ctrl Pts',(-20.9465618823528,20.6024933823517,-15.5728472703339));
#58617=CARTESIAN_POINT('Ctrl Pts',(-20.8596931182755,20.6792226459343,-15.5669832189785));
#58618=CARTESIAN_POINT('Ctrl Pts',(-20.7763054943334,20.7597186483438,-15.561119167623));
#58619=CARTESIAN_POINT('Ctrl Pts',(-20.6967239966534,20.8436192170933,-15.5552551162676));
#58620=CARTESIAN_POINT('Ctrl Pts',(-20.6170252117318,20.9276434385328,-15.549382422471));
#58621=CARTESIAN_POINT('Ctrl Pts',(-20.5411440184189,21.0150819295381,-15.5435097286744));
#58622=CARTESIAN_POINT('Ctrl Pts',(-20.4693644673144,21.105540332935,-15.5376370348779));
#58623=CARTESIAN_POINT('Ctrl Pts',(-20.449712426947,21.130306330601,-15.5360291895545));
#58624=CARTESIAN_POINT('Ctrl Pts',(-20.4303675788492,21.1552985329118,-15.5344213442312));
#58625=CARTESIAN_POINT('Ctrl Pts',(-20.4113351655613,21.1805085015109,-15.5328134989078));
#58626=CARTESIAN_POINT('Ctrl Pts',(-20.3418235146362,21.2725822974392,-15.5269412019391));
#58627=CARTESIAN_POINT('Ctrl Pts',(-20.2762500456629,21.3678714106469,-15.5210689049704));
#58628=CARTESIAN_POINT('Ctrl Pts',(-20.2149266659304,21.4660043772829,-15.5151966080017));
#58629=CARTESIAN_POINT('Ctrl Pts',(-20.1536827564278,21.5640101713876,-15.5093319210635));
#58630=CARTESIAN_POINT('Ctrl Pts',(-20.0966782002179,21.6648521426388,-15.5034672341253));
#58631=CARTESIAN_POINT('Ctrl Pts',(-20.0441839742809,21.7681267587147,-15.4976025471871));
#58632=CARTESIAN_POINT('Ctrl Pts',(-19.9917437353691,21.871295163313,-15.4917438917123));
#58633=CARTESIAN_POINT('Ctrl Pts',(-19.943804786518,21.9768908701874,-15.4858852362375));
#58634=CARTESIAN_POINT('Ctrl Pts',(-19.9005938196463,22.0844830117585,-15.4800265807627));
#58635=CARTESIAN_POINT('Ctrl Pts',(-19.8556949943487,22.1962777971454,-15.4739390810447));
#58636=CARTESIAN_POINT('Ctrl Pts',(-19.8159012800347,22.3102277761564,-15.4678515813268));
#58637=CARTESIAN_POINT('Ctrl Pts',(-19.7814135481827,22.4258230246267,-15.4617640816089));
#58638=CARTESIAN_POINT('Ctrl Pts',(-19.7482607374031,22.5369439129474,-15.4559122115255));
#58639=CARTESIAN_POINT('Ctrl Pts',(-19.7200109173269,22.6495846386329,-15.4500603414421));
#58640=CARTESIAN_POINT('Ctrl Pts',(-19.6967924561964,22.7632744846406,-15.4442084713588));
#58641=CARTESIAN_POINT('Ctrl Pts',(-19.6735775302877,22.8769470203355,-15.4383574922758));
#58642=CARTESIAN_POINT('Ctrl Pts',(-19.6553925228255,22.9916679538306,-15.4325065131928));
#58643=CARTESIAN_POINT('Ctrl Pts',(-19.642314884938,23.1069553976346,-15.4266555341099));
#58644=CARTESIAN_POINT('Ctrl Pts',(-19.6292360712449,23.2222532068893,-15.4208040289676));
#58645=CARTESIAN_POINT('Ctrl Pts',(-19.6212655865731,23.3381172169335,-15.4149525238253));
#58646=CARTESIAN_POINT('Ctrl Pts',(-19.6184290332188,23.4540601367925,-15.409101018683));
#58647=CARTESIAN_POINT('Ctrl Pts',(-19.6155915379069,23.5700415587711,-15.4032475703832));
#58648=CARTESIAN_POINT('Ctrl Pts',(-19.6178913740379,23.6861015296295,-15.3973941220835));
#58649=CARTESIAN_POINT('Ctrl Pts',(-19.6253020328076,23.8017531903207,-15.3915406737837));
#58650=CARTESIAN_POINT('Ctrl Pts',(-19.6327211191055,23.9175363720635,-15.3856805688421));
#58651=CARTESIAN_POINT('Ctrl Pts',(-19.6452626023982,24.0329099040543,-15.3798204639006));
#58652=CARTESIAN_POINT('Ctrl Pts',(-19.6628481268706,24.1473923757494,-15.3739603589591));
#58653=CARTESIAN_POINT('Ctrl Pts',(-19.6804454940931,24.2619519442239,-15.3680963076036));
#58654=CARTESIAN_POINT('Ctrl Pts',(-19.7030935857089,24.3756188531146,-15.3622322562482));
#58655=CARTESIAN_POINT('Ctrl Pts',(-19.7306633687071,24.4879239165574,-15.3563682048927));
#58656=CARTESIAN_POINT('Ctrl Pts',(-19.7582737840619,24.6003944952455,-15.3504955110962));
#58657=CARTESIAN_POINT('Ctrl Pts',(-19.7908202517915,24.7114988275022,-15.3446228172996));
#58658=CARTESIAN_POINT('Ctrl Pts',(-19.8281245339796,24.8207847700214,-15.338750123503));
#58659=CARTESIAN_POINT('Ctrl Pts',(-19.8383378224184,24.8507054329533,-15.3371422781797));
#58660=CARTESIAN_POINT('Ctrl Pts',(-19.8489074710648,24.8804899230745,-15.3355344328563));
#58661=CARTESIAN_POINT('Ctrl Pts',(-19.859829214403,24.9101292684588,-15.3339265875329));
#58662=CARTESIAN_POINT('Ctrl Pts',(-19.8997184496214,25.0183803766504,-15.3280542905642));
#58663=CARTESIAN_POINT('Ctrl Pts',(-19.9444415395107,25.1250562415868,-15.3221819935955));
#58664=CARTESIAN_POINT('Ctrl Pts',(-19.9938545644128,25.2296936584732,-15.3163096966268));
#58665=CARTESIAN_POINT('Ctrl Pts',(-20.0432035539589,25.3341954735775,-15.3104450096886));
#58666=CARTESIAN_POINT('Ctrl Pts',(-20.097230217098,25.4366637236095,-15.3045803227504));
#58667=CARTESIAN_POINT('Ctrl Pts',(-20.1557415298627,25.5366523047623,-15.2987156358122));
#58668=CARTESIAN_POINT('Ctrl Pts',(-20.2141926674051,25.6365380539187,-15.2928569803373));
#58669=CARTESIAN_POINT('Ctrl Pts',(-20.2771190731792,25.7339488520042,-15.2869983248625));
#58670=CARTESIAN_POINT('Ctrl Pts',(-20.3442807876536,25.8284610771116,-15.2811396693877));
#58671=CARTESIAN_POINT('Ctrl Pts',(-20.4140658978505,25.9266650329769,-15.2750521696698));
#58672=CARTESIAN_POINT('Ctrl Pts',(-20.4884237375113,26.0217389468359,-15.2689646699519));
#58673=CARTESIAN_POINT('Ctrl Pts',(-20.5670338784302,26.1132381865151,-15.262877170234));
#58674=CARTESIAN_POINT('Ctrl Pts',(-20.6426012465145,26.2011957533564,-15.2570253001506));
#58675=CARTESIAN_POINT('Ctrl Pts',(-20.7220975536018,26.2858498883814,-15.2511734300672));
#58676=CARTESIAN_POINT('Ctrl Pts',(-20.8051961660232,26.3668381507175,-15.2453215599838));
#58677=CARTESIAN_POINT('Ctrl Pts',(-20.8882821259252,26.4478140818543,-15.2394705809008));
#58678=CARTESIAN_POINT('Ctrl Pts',(-20.9749690046405,26.5251249616645,-15.2336196018178));
#58679=CARTESIAN_POINT('Ctrl Pts',(-21.0648932477556,26.5984451485969,-15.2277686227348));
#58680=CARTESIAN_POINT('Ctrl Pts',(-21.1548255759256,26.6717719277198,-15.2219171175925));
#58681=CARTESIAN_POINT('Ctrl Pts',(-21.247995526713,26.7411070394578,-15.2160656124502));
#58682=CARTESIAN_POINT('Ctrl Pts',(-21.3440069731715,26.8061655427402,-15.2102141073079));
#58683=CARTESIAN_POINT('Ctrl Pts',(-21.4400503029412,26.8712456505352,-15.2043606590081));
#58684=CARTESIAN_POINT('Ctrl Pts',(-21.5389366626332,26.9320460941914,-15.1985072107084));
#58685=CARTESIAN_POINT('Ctrl Pts',(-21.6402421204302,26.9883260080561,-15.1926537624086));
#58686=CARTESIAN_POINT('Ctrl Pts',(-21.7416627845308,27.0446699244038,-15.186793657467));
#58687=CARTESIAN_POINT('Ctrl Pts',(-21.8455076761515,27.0964828491577,-15.1809335525255));
#58688=CARTESIAN_POINT('Ctrl Pts',(-21.9513294218846,27.1435704815724,-15.1750734475839));
#58689=CARTESIAN_POINT('Ctrl Pts',(-22.0572224319403,27.1906898245604,-15.1692093962285));
#58690=CARTESIAN_POINT('Ctrl Pts',(-22.1650945631609,27.2330773880264,-15.163345344873));
#58691=CARTESIAN_POINT('Ctrl Pts',(-22.2744813337942,27.2705881147578,-15.1574812935176));
#58692=CARTESIAN_POINT('Ctrl Pts',(-22.3840293186918,27.3081541248125,-15.151608599721));
#58693=CARTESIAN_POINT('Ctrl Pts',(-22.495096003106,27.3408288370704,-15.1457359059244));
#58694=CARTESIAN_POINT('Ctrl Pts',(-22.6072046461377,27.3685178034567,-15.1398632121278));
#58695=CARTESIAN_POINT('Ctrl Pts',(-22.6378981172501,27.3760985792731,-15.1382553668046));
#58696=CARTESIAN_POINT('Ctrl Pts',(-22.6686696516916,27.3833059360911,-15.1366475214813));
#58697=CARTESIAN_POINT('Ctrl Pts',(-22.6995093955379,27.3901386128538,-15.135039676158));
#58698=CARTESIAN_POINT('Ctrl Pts',(-22.8121446917831,27.4150934430607,-15.1291673791893));
#58699=CARTESIAN_POINT('Ctrl Pts',(-22.9260676128191,27.4351299844707,-15.1232950822206));
#58700=CARTESIAN_POINT('Ctrl Pts',(-23.0408106620039,27.4501189372787,-15.1174227852519));
#58701=CARTESIAN_POINT('Ctrl Pts',(-23.1554050133099,27.4650884655942,-15.1115580983137));
#58702=CARTESIAN_POINT('Ctrl Pts',(-23.2708169730786,27.4750233605024,-15.1056934113755));
#58703=CARTESIAN_POINT('Ctrl Pts',(-23.3865668890551,27.4798448782861,-15.0998287244373));
#58704=CARTESIAN_POINT('Ctrl Pts',(-23.502197763489,27.4846614374407,-15.0939700689625));
#58705=CARTESIAN_POINT('Ctrl Pts',(-23.6181654922608,27.4843750623702,-15.0881114134877));
#58706=CARTESIAN_POINT('Ctrl Pts',(-23.7339839668532,27.4789586494554,-15.0822527580129));
#58707=CARTESIAN_POINT('Ctrl Pts',(-23.8543264130753,27.4733306666814,-15.076165258295));
#58708=CARTESIAN_POINT('Ctrl Pts',(-23.9745072565679,27.4621636494907,-15.0700777585771));
#58709=CARTESIAN_POINT('Ctrl Pts',(-24.0939792157942,27.44548683697,-15.0639902588592));
#58710=CARTESIAN_POINT('Ctrl Pts',(-24.2088267585288,27.4294555359765,-15.0581383887758));
#58711=CARTESIAN_POINT('Ctrl Pts',(-24.3230188267413,27.40833310774,-15.0522865186924));
#58712=CARTESIAN_POINT('Ctrl Pts',(-24.4360739334993,27.3821984399899,-15.0464346486091));
#58713=CARTESIAN_POINT('Ctrl Pts',(-24.5491118265893,27.3560677514806,-15.0405836695261));
#58714=CARTESIAN_POINT('Ctrl Pts',(-24.6610126997775,27.324926433942,-15.0347326904432));
#58715=CARTESIAN_POINT('Ctrl Pts',(-24.7713060687906,27.2889043287387,-15.0288817113602));
#58716=CARTESIAN_POINT('Ctrl Pts',(-24.881609354239,27.2528789848015,-15.0230302062179));
#58717=CARTESIAN_POINT('Ctrl Pts',(-24.9903044552207,27.2119721091944,-15.0171787010756));
#58718=CARTESIAN_POINT('Ctrl Pts',(-25.0969375226245,27.1663629474353,-15.0113271959334));
#58719=CARTESIAN_POINT('Ctrl Pts',(-25.2036060005487,27.1207386398664,-15.0054737476336));
#58720=CARTESIAN_POINT('Ctrl Pts',(-25.3082107034252,27.0704091036279,-14.9996202993338));
#58721=CARTESIAN_POINT('Ctrl Pts',(-25.4103198338202,27.0156008015744,-14.9937668510341));
#58722=CARTESIAN_POINT('Ctrl Pts',(-25.5125450844689,26.9607301705801,-14.9879067460925));
#58723=CARTESIAN_POINT('Ctrl Pts',(-25.6122687336126,26.9013708032601,-14.982046641151));
#58724=CARTESIAN_POINT('Ctrl Pts',(-25.7090854884818,26.8377940545784,-14.9761865362095));
#58725=CARTESIAN_POINT('Ctrl Pts',(-25.8059674433759,26.7741744909356,-14.9703224848541));
#58726=CARTESIAN_POINT('Ctrl Pts',(-25.8999382716577,26.7063321320246,-14.9644584334986));
#58727=CARTESIAN_POINT('Ctrl Pts',(-25.9906248621826,26.6345793445638,-14.9585943821432));
#58728=CARTESIAN_POINT('Ctrl Pts',(-26.081445106639,26.5627208078177,-14.9527216883466));
#58729=CARTESIAN_POINT('Ctrl Pts',(-26.1689711416627,26.4869406098711,-14.9468489945501));
#58730=CARTESIAN_POINT('Ctrl Pts',(-26.2528658078369,26.4075887876531,-14.9409763007535));
#58731=CARTESIAN_POINT('Ctrl Pts',(-26.2758347640507,26.3858635861221,-14.9393684554301));
#58732=CARTESIAN_POINT('Ctrl Pts',(-26.2985317531343,26.3638708598036,-14.9377606101066));
#58733=CARTESIAN_POINT('Ctrl Pts',(-26.3209503876758,26.3416182173146,-14.9361527647832));
#58734=CARTESIAN_POINT('Ctrl Pts',(-26.4016830745772,26.2614832913686,-14.9303626854257));
#58735=CARTESIAN_POINT('Ctrl Pts',(-26.4790900040286,26.1776901938045,-14.9245726060681));
#58736=CARTESIAN_POINT('Ctrl Pts',(-26.552814138775,26.0905503086653,-14.9187825267106));
#58737=CARTESIAN_POINT('Ctrl Pts',(-26.6268868880288,26.0029983708348,-14.9129650681824));
#58738=CARTESIAN_POINT('Ctrl Pts',(-26.697241562853,25.9120681579657,-14.9071476096542));
#58739=CARTESIAN_POINT('Ctrl Pts',(-26.7635508773111,25.8181155659305,-14.9013301511261));
#58740=CARTESIAN_POINT('Ctrl Pts',(-26.829383469992,25.7248384332484,-14.895554516423));
#58741=CARTESIAN_POINT('Ctrl Pts',(-26.8912284090564,25.6285825744804,-14.8897788817199));
#58742=CARTESIAN_POINT('Ctrl Pts',(-26.9488042042189,25.529731132028,-14.8840032470168));
#58743=CARTESIAN_POINT('Ctrl Pts',(-27.0063428259051,25.430943512433,-14.8782313413186));
#58744=CARTESIAN_POINT('Ctrl Pts',(-27.059617567142,25.3295640059362,-14.8724594356204));
#58745=CARTESIAN_POINT('Ctrl Pts',(-27.1083901535948,25.2260047996669,-14.8666875299221));
#58746=CARTESIAN_POINT('Ctrl Pts',(-27.157143839213,25.1224857256844,-14.8609178610098));
#58747=CARTESIAN_POINT('Ctrl Pts',(-27.2013986573955,25.0167890160884,-14.8551481920975));
#58748=CARTESIAN_POINT('Ctrl Pts',(-27.2409626339126,24.9093507405751,-14.8493785231852));
#58749=CARTESIAN_POINT('Ctrl Pts',(-27.2810860317898,24.8003933238754,-14.8435272730894));
#58750=CARTESIAN_POINT('Ctrl Pts',(-27.3163847168276,24.6896451152041,-14.8376760229935));
#58751=CARTESIAN_POINT('Ctrl Pts',(-27.3467096178911,24.577580421253,-14.8318247728976));
#58752=CARTESIAN_POINT('Ctrl Pts',(-27.3766216786034,24.4670413655066,-14.8260531811703));
#58753=CARTESIAN_POINT('Ctrl Pts',(-27.4016944754199,24.3552218779928,-14.820281589443));
#58754=CARTESIAN_POINT('Ctrl Pts',(-27.4218359661124,24.2425896680222,-14.8145099977156));
#58755=CARTESIAN_POINT('Ctrl Pts',(-27.4423944401166,24.1276256667932,-14.8086189184355));
#58756=CARTESIAN_POINT('Ctrl Pts',(-27.4578150786415,24.011815377055,-14.8027278391554));
#58757=CARTESIAN_POINT('Ctrl Pts',(-27.4680555937978,23.8956626742372,-14.7968367598752));
#58758=CARTESIAN_POINT('Ctrl Pts',(-27.4782961089542,23.7795099714194,-14.7909456805951));
#58759=CARTESIAN_POINT('Ctrl Pts',(-27.4833565176931,23.6630153255504,-14.7850546013149));
#58760=CARTESIAN_POINT('Ctrl Pts',(-27.4832509111211,23.5466821780573,-14.7791635220348));
#58761=CARTESIAN_POINT('',(-27.4888203141544,23.551993354051,-13.5291635220348));
#58762=CARTESIAN_POINT('Ctrl Pts',(-27.4841329879773,23.5466813773129,-14.7791635220348));
#58763=CARTESIAN_POINT('Ctrl Pts',(-27.4866979788519,23.2708277947411,-14.7651976324926));
#58764=CARTESIAN_POINT('Ctrl Pts',(-27.3342151592236,21.6883218579646,-14.6849361058252));
#58765=CARTESIAN_POINT('Ctrl Pts',(-25.1911129410817,19.1972848142637,-14.5383789420335));
#58766=CARTESIAN_POINT('Ctrl Pts',(-20.7749823681344,19.8168055518416,-14.3394920306583));
#58767=CARTESIAN_POINT('Ctrl Pts',(-18.909089771392,23.8670475198046,-14.1406051192836));
#58768=CARTESIAN_POINT('Ctrl Pts',(-21.3080322456564,27.6261817534765,-13.9417182079087));
#58769=CARTESIAN_POINT('Ctrl Pts',(-25.7673850538621,27.6398826141424,-13.7428312965338));
#58770=CARTESIAN_POINT('Ctrl Pts',(-27.4420482966652,25.0509108913852,-13.6053130679092));
#58771=CARTESIAN_POINT('Ctrl Pts',(-27.4893561445465,23.6490092491261,-13.5340904764095));
#58772=CARTESIAN_POINT('Ctrl Pts',(-27.4888203141544,23.551993354051,-13.5291635220348));
#58773=CARTESIAN_POINT('',(-27.4787742047217,23.5529763597193,-12.2791635220348));
#58774=CARTESIAN_POINT('Ctrl Pts',(-27.4888203141544,23.551993354051,-13.5291635220348));
#58775=CARTESIAN_POINT('Ctrl Pts',(-27.4821461696749,22.3435921321586,-13.4677948392845));
#58776=CARTESIAN_POINT('Ctrl Pts',(-26.2391084225207,19.817910182807,-13.3401305194094));
#58777=CARTESIAN_POINT('Ctrl Pts',(-21.9361708563877,19.1872843702759,-13.1461705624091));
#58778=CARTESIAN_POINT('Ctrl Pts',(-19.0071346432534,22.5498372759953,-12.9472836510342));
#58779=CARTESIAN_POINT('Ctrl Pts',(-20.2528385767197,26.8316869804742,-12.7483967396594));
#58780=CARTESIAN_POINT('Ctrl Pts',(-24.5285863602099,28.0981766462875,-12.5495098282844));
#58781=CARTESIAN_POINT('Ctrl Pts',(-27.1841649778446,25.8075615147313,-12.3930987557429));
#58782=CARTESIAN_POINT('Ctrl Pts',(-27.4817723373124,24.0250936006054,-12.3029833203264));
#58783=CARTESIAN_POINT('Ctrl Pts',(-27.4787742047217,23.5529763597193,-12.2791635220348));
#58784=CARTESIAN_POINT('',(-27.4823549449185,23.5474739030226,-11.0291634828679));
#58785=CARTESIAN_POINT('Ctrl Pts',(-27.4787742047217,23.5529763597193,-12.2791635220348));
#58786=CARTESIAN_POINT('Ctrl Pts',(-27.4734278875462,22.71108947265,-12.2366876832014));
#58787=CARTESIAN_POINT('Ctrl Pts',(-26.7947582611164,20.547334820768,-12.127916207243));
#58788=CARTESIAN_POINT('Ctrl Pts',(-23.2274849901484,18.9095013051977,-11.9528490941598));
#58789=CARTESIAN_POINT('Ctrl Pts',(-19.4714411218787,21.3132795065398,-11.7539621827848));
#58790=CARTESIAN_POINT('Ctrl Pts',(-19.4634791130517,25.7726462539626,-11.55507527141));
#58791=CARTESIAN_POINT('Ctrl Pts',(-23.2109153747127,28.1898215985376,-11.356188360035));
#58792=CARTESIAN_POINT('Ctrl Pts',(-26.7888475756172,26.5625387526775,-11.1808844435768));
#58793=CARTESIAN_POINT('Ctrl Pts',(-27.4733876852228,24.3940033727517,-11.0718761642433));
#58794=CARTESIAN_POINT('Ctrl Pts',(-27.4788743631229,23.5474771390092,-11.0291635220348));
#58795=CARTESIAN_POINT('',(-27.4847851822191,23.5485896828163,-9.7791635220348));
#58796=CARTESIAN_POINT('Ctrl Pts',(-27.4832515495671,23.5474730694262,-11.0291634727785));
#58797=CARTESIAN_POINT('Ctrl Pts',(-27.4831577687811,23.4147712357825,-11.0224752375737));
#58798=CARTESIAN_POINT('Ctrl Pts',(-27.4763438388193,23.2823366808379,-11.015787002369));
#58799=CARTESIAN_POINT('Ctrl Pts',(-27.4629146449167,23.1507976684699,-11.0090987671643));
#58800=CARTESIAN_POINT('Ctrl Pts',(-27.4494191222458,23.0186089655308,-11.0023774977801));
#58801=CARTESIAN_POINT('Ctrl Pts',(-27.4292429435521,22.8873248327967,-10.9956562283959));
#58802=CARTESIAN_POINT('Ctrl Pts',(-27.4025420174753,22.7575642463385,-10.9889349590116));
#58803=CARTESIAN_POINT('Ctrl Pts',(-27.375678109144,22.6270116022238,-10.982172663049));
#58804=CARTESIAN_POINT('Ctrl Pts',(-27.3422096534684,22.4980013167981,-10.9754103670863));
#58805=CARTESIAN_POINT('Ctrl Pts',(-27.3023437719518,22.3711425602402,-10.9686480711237));
#58806=CARTESIAN_POINT('Ctrl Pts',(-27.2822337950174,22.3071498283289,-10.9652368931776));
#58807=CARTESIAN_POINT('Ctrl Pts',(-27.2604966784544,22.2437042265049,-10.9618257152314));
#58808=CARTESIAN_POINT('Ctrl Pts',(-27.2371635166089,22.1808817311746,-10.9584145372853));
#58809=CARTESIAN_POINT('Ctrl Pts',(-27.1969957922217,22.072733650154,-10.9525422403166));
#58810=CARTESIAN_POINT('Ctrl Pts',(-27.151998283603,21.966173248751,-10.9466699433479));
#58811=CARTESIAN_POINT('Ctrl Pts',(-27.1023161021502,21.8616633597997,-10.9407976463792));
#58812=CARTESIAN_POINT('Ctrl Pts',(-27.052698304859,21.7572889073645,-10.934932959441));
#58813=CARTESIAN_POINT('Ctrl Pts',(-26.9984080835449,21.6549600528605,-10.9290682725029));
#58814=CARTESIAN_POINT('Ctrl Pts',(-26.9396396097369,21.5551224018036,-10.9232035855647));
#58815=CARTESIAN_POINT('Ctrl Pts',(-26.8809315756252,21.4553874275208,-10.9173449300899));
#58816=CARTESIAN_POINT('Ctrl Pts',(-26.8177546582395,21.3581389147464,-10.9114862746151));
#58817=CARTESIAN_POINT('Ctrl Pts',(-26.7503499066524,21.2637998663661,-10.9056276191403));
#58818=CARTESIAN_POINT('Ctrl Pts',(-26.6803122660988,21.1657758516631,-10.8995401194223));
#58819=CARTESIAN_POINT('Ctrl Pts',(-26.6057099674625,21.0708936380837,-10.8934526197044));
#58820=CARTESIAN_POINT('Ctrl Pts',(-26.5268645823014,20.979597031597,-10.8873651199865));
#58821=CARTESIAN_POINT('Ctrl Pts',(-26.4510710756044,20.8918342545996,-10.8815132499032));
#58822=CARTESIAN_POINT('Ctrl Pts',(-26.3713571454313,20.8073850109463,-10.8756613798198));
#58823=CARTESIAN_POINT('Ctrl Pts',(-26.288050357235,20.7266108996056,-10.8698095097364));
#58824=CARTESIAN_POINT('Ctrl Pts',(-26.2047562532546,20.6458490868577,-10.8639585306534));
#58825=CARTESIAN_POINT('Ctrl Pts',(-26.1178706756531,20.5687615814942,-10.8581075515705));
#58826=CARTESIAN_POINT('Ctrl Pts',(-26.0277580157897,20.4956730882557,-10.8522565724875));
#58827=CARTESIAN_POINT('Ctrl Pts',(-25.9376372539309,20.4225780236584,-10.8464050673452));
#58828=CARTESIAN_POINT('Ctrl Pts',(-25.8442891541018,20.3534829463545,-10.840553562203));
#58829=CARTESIAN_POINT('Ctrl Pts',(-25.7481105753298,20.2886717769027,-10.8347020570607));
#58830=CARTESIAN_POINT('Ctrl Pts',(-25.6519000577456,20.2238390850725,-10.8288486087609));
#58831=CARTESIAN_POINT('Ctrl Pts',(-25.5528575348373,20.1632933607165,-10.8229951604612));
#58832=CARTESIAN_POINT('Ctrl Pts',(-25.4514075569683,20.1072743775557,-10.8171417121614));
#58833=CARTESIAN_POINT('Ctrl Pts',(-25.349842208445,20.0511916886468,-10.8112816072199));
#58834=CARTESIAN_POINT('Ctrl Pts',(-25.24586430249,19.9996462159032,-10.8054215022784));
#58835=CARTESIAN_POINT('Ctrl Pts',(-25.1399217111285,19.9528311079579,-10.7995613973369));
#58836=CARTESIAN_POINT('Ctrl Pts',(-25.0339077740625,19.9059844729675,-10.7936973459814));
#58837=CARTESIAN_POINT('Ctrl Pts',(-24.925926901242,19.863874695772,-10.787833294626));
#58838=CARTESIAN_POINT('Ctrl Pts',(-24.8164439462352,19.8266456376004,-10.7819692432706));
#58839=CARTESIAN_POINT('Ctrl Pts',(-24.7067996352075,19.7893617112287,-10.776096549474));
#58840=CARTESIAN_POINT('Ctrl Pts',(-24.5956492191233,19.7569729753454,-10.7702238556775));
#58841=CARTESIAN_POINT('Ctrl Pts',(-24.4834696803974,19.7295726506565,-10.7643511618809));
#58842=CARTESIAN_POINT('Ctrl Pts',(-24.4527567992256,19.7220709001074,-10.7627433165574));
#58843=CARTESIAN_POINT('Ctrl Pts',(-24.4219668161049,19.7149427682426,-10.7611354712339));
#58844=CARTESIAN_POINT('Ctrl Pts',(-24.3911095881728,19.7081894907525,-10.7595276259104));
#58845=CARTESIAN_POINT('Ctrl Pts',(-24.2784104352126,19.6835246487091,-10.7536553289417));
#58846=CARTESIAN_POINT('Ctrl Pts',(-24.164436320627,19.663781393315,-10.747783031973));
#58847=CARTESIAN_POINT('Ctrl Pts',(-24.0496550723067,19.6490878206842,-10.7419107350043));
#58848=CARTESIAN_POINT('Ctrl Pts',(-23.9350225713685,19.6344132897566,-10.7360460480661));
#58849=CARTESIAN_POINT('Ctrl Pts',(-23.8195854230289,19.6247754799554,-10.7301813611279));
#58850=CARTESIAN_POINT('Ctrl Pts',(-23.7038234806278,19.6202519001874,-10.7243166741897));
#58851=CARTESIAN_POINT('Ctrl Pts',(-23.5881805921378,19.615732972638,-10.7184580187149));
#58852=CARTESIAN_POINT('Ctrl Pts',(-23.4722139845741,19.616317829421,-10.71259936324));
#58853=CARTESIAN_POINT('Ctrl Pts',(-23.3564098346046,19.6220323228993,-10.7067407077652));
#58854=CARTESIAN_POINT('Ctrl Pts',(-23.2360822725383,19.627970029526,-10.7006532080473));
#58855=CARTESIAN_POINT('Ctrl Pts',(-23.115930569268,19.6394463362824,-10.6945657083294));
#58856=CARTESIAN_POINT('Ctrl Pts',(-22.9965019292611,19.6564305955619,-10.6884782086115));
#58857=CARTESIAN_POINT('Ctrl Pts',(-22.8816960289827,19.6727574429332,-10.6826263385281));
#58858=CARTESIAN_POINT('Ctrl Pts',(-22.7675587048147,19.6941737135958,-10.6767744684447));
#58859=CARTESIAN_POINT('Ctrl Pts',(-22.6545712390499,19.7205992808101,-10.6709225983613));
#58860=CARTESIAN_POINT('Ctrl Pts',(-22.5416009766541,19.7470208244916,-10.6650716192783));
#58861=CARTESIAN_POINT('Ctrl Pts',(-22.4297806269636,19.7784500540953,-10.6592206401954));
#58862=CARTESIAN_POINT('Ctrl Pts',(-22.3195803385021,19.8147559177346,-10.6533696611124));
#58863=CARTESIAN_POINT('Ctrl Pts',(-22.2093701419741,19.8510650456204,-10.6475181559701));
#58864=CARTESIAN_POINT('Ctrl Pts',(-22.1007806888794,19.8922515497934,-10.6416666508278));
#58865=CARTESIAN_POINT('Ctrl Pts',(-21.994265365476,19.9381350171933,-10.6358151456855));
#58866=CARTESIAN_POINT('Ctrl Pts',(-21.8877146706524,19.9840337214939,-10.6299616973857));
#58867=CARTESIAN_POINT('Ctrl Pts',(-21.7832398545578,20.0346323270471,-10.6241082490859));
#58868=CARTESIAN_POINT('Ctrl Pts',(-21.681272130316,20.0897032603698,-10.6182548007862));
#58869=CARTESIAN_POINT('Ctrl Pts',(-21.57918844663,20.144836821302,-10.6123946958446));
#58870=CARTESIAN_POINT('Ctrl Pts',(-21.479617909463,20.2044526649637,-10.6065345909031));
#58871=CARTESIAN_POINT('Ctrl Pts',(-21.3829651118169,20.2682783941298,-10.6006744859615));
#58872=CARTESIAN_POINT('Ctrl Pts',(-21.286247224561,20.3321471059297,-10.5948104346061));
#58873=CARTESIAN_POINT('Ctrl Pts',(-21.1924513230845,20.4002311062293,-10.5889463832507));
#58874=CARTESIAN_POINT('Ctrl Pts',(-21.1019497133133,20.4722170690155,-10.5830823318952));
#58875=CARTESIAN_POINT('Ctrl Pts',(-21.0113147222349,20.5443091247411,-10.5772096380986));
#58876=CARTESIAN_POINT('Ctrl Pts',(-20.9239840234159,20.6203143499014,-10.5713369443021));
#58877=CARTESIAN_POINT('Ctrl Pts',(-20.8402938742161,20.6998818409314,-10.5654642505055));
#58878=CARTESIAN_POINT('Ctrl Pts',(-20.8173809113305,20.7216660889738,-10.5638564051822));
#58879=CARTESIAN_POINT('Ctrl Pts',(-20.7947406032408,20.743717160917,-10.5622485598589));
#58880=CARTESIAN_POINT('Ctrl Pts',(-20.7723793177545,20.766027431729,-10.5606407145355));
#58881=CARTESIAN_POINT('Ctrl Pts',(-20.6907097024792,20.8475107272674,-10.5547684175668));
#58882=CARTESIAN_POINT('Ctrl Pts',(-20.6124915298197,20.9327269956377,-10.5488961205981));
#58883=CARTESIAN_POINT('Ctrl Pts',(-20.5380854499933,21.0213518867661,-10.5430238236294));
#58884=CARTESIAN_POINT('Ctrl Pts',(-20.4637757945373,21.109861927074,-10.5371591366912));
#58885=CARTESIAN_POINT('Ctrl Pts',(-20.3932686710403,21.2017714920319,-10.531294449753));
#58886=CARTESIAN_POINT('Ctrl Pts',(-20.3268886701188,21.2967187698237,-10.5254297628148));
#58887=CARTESIAN_POINT('Ctrl Pts',(-20.2605769368729,21.3915684002841,-10.5195711073399));
#58888=CARTESIAN_POINT('Ctrl Pts',(-20.1983841191357,21.4894491928289,-10.5137124518651));
#58889=CARTESIAN_POINT('Ctrl Pts',(-20.1405947660332,21.5899660931685,-10.5078537963903));
#58890=CARTESIAN_POINT('Ctrl Pts',(-20.0805481098984,21.6944092721694,-10.5017662966724));
#58891=CARTESIAN_POINT('Ctrl Pts',(-20.0252562301151,21.8016983463826,-10.4956787969545));
#58892=CARTESIAN_POINT('Ctrl Pts',(-19.9749891295499,21.9113563771781,-10.4895912972366));
#58893=CARTESIAN_POINT('Ctrl Pts',(-19.9266677241112,22.0167698604725,-10.4837394271532));
#58894=CARTESIAN_POINT('Ctrl Pts',(-19.8829895296096,22.1243719085128,-10.4778875570697));
#58895=CARTESIAN_POINT('Ctrl Pts',(-19.8441472875572,22.2337142985312,-10.4720356869863));
#58896=CARTESIAN_POINT('Ctrl Pts',(-19.8053109595893,22.3430400401764,-10.4661847079034));
#58897=CARTESIAN_POINT('Ctrl Pts',(-19.7713092583735,22.4541052075011,-10.4603337288204));
#58898=CARTESIAN_POINT('Ctrl Pts',(-19.7422860629667,22.5664434175634,-10.4544827497374));
#58899=CARTESIAN_POINT('Ctrl Pts',(-19.7132602580953,22.6787917279119,-10.4486312445951));
#58900=CARTESIAN_POINT('Ctrl Pts',(-19.689213952262,22.7924129082668,-10.4427797394528));
#58901=CARTESIAN_POINT('Ctrl Pts',(-19.6702404354251,22.9068279962544,-10.4369282343105));
#58902=CARTESIAN_POINT('Ctrl Pts',(-19.6512606178964,23.0212810790022,-10.4310747860107));
#58903=CARTESIAN_POINT('Ctrl Pts',(-19.6373570066032,23.1365281860155,-10.4252213377109));
#58904=CARTESIAN_POINT('Ctrl Pts',(-19.6285712291301,23.2520835173433,-10.4193678894112));
#58905=CARTESIAN_POINT('Ctrl Pts',(-19.6197754603201,23.3677702601752,-10.4135077844696));
#58906=CARTESIAN_POINT('Ctrl Pts',(-19.6161091734087,23.4837655145072,-10.4076476795281));
#58907=CARTESIAN_POINT('Ctrl Pts',(-19.6175618957094,23.5995816472105,-10.4017875745865));
#58908=CARTESIAN_POINT('Ctrl Pts',(-19.6190155963277,23.7154757748305,-10.3959235232311));
#58909=CARTESIAN_POINT('Ctrl Pts',(-19.6255951470715,23.8311901289213,-10.3900594718756));
#58910=CARTESIAN_POINT('Ctrl Pts',(-19.637238188645,23.946242116268,-10.3841954205201));
#58911=CARTESIAN_POINT('Ctrl Pts',(-19.6488983897376,24.0614636672775,-10.3783227267236));
#58912=CARTESIAN_POINT('Ctrl Pts',(-19.6656369159767,24.1760204957395,-10.372450032927));
#58913=CARTESIAN_POINT('Ctrl Pts',(-19.6873403076637,24.2894400244426,-10.3665773391304));
#58914=CARTESIAN_POINT('Ctrl Pts',(-19.6932823332539,24.3204923941232,-10.3649694938071));
#58915=CARTESIAN_POINT('Ctrl Pts',(-19.6995962237446,24.3514596043792,-10.3633616484839));
#58916=CARTESIAN_POINT('Ctrl Pts',(-19.7062790061382,24.3823321762144,-10.3617538031606));
#58917=CARTESIAN_POINT('Ctrl Pts',(-19.7306863805445,24.4950873693786,-10.3558815061919));
#58918=CARTESIAN_POINT('Ctrl Pts',(-19.7601000186777,24.6069566360287,-10.3500092092232));
#58919=CARTESIAN_POINT('Ctrl Pts',(-19.7944419861104,24.7174612301205,-10.3441369122545));
#58920=CARTESIAN_POINT('Ctrl Pts',(-19.8287394490808,24.8278226190343,-10.3382722253163));
#58921=CARTESIAN_POINT('Ctrl Pts',(-19.8679524189018,24.9368224612007,-10.3324075383781));
#58922=CARTESIAN_POINT('Ctrl Pts',(-19.9119519522107,25.0439920984628,-10.3265428514399));
#58923=CARTESIAN_POINT('Ctrl Pts',(-19.955906234754,25.1510515184619,-10.3206841959651));
#58924=CARTESIAN_POINT('Ctrl Pts',(-20.0046371332621,25.2562840973421,-10.3148255404903));
#58925=CARTESIAN_POINT('Ctrl Pts',(-20.0579660927985,25.3592368955584,-10.3089668850155));
#58926=CARTESIAN_POINT('Ctrl Pts',(-20.1133781284661,25.466211120753,-10.3028793852976));
#58927=CARTESIAN_POINT('Ctrl Pts',(-20.1737546217122,25.5707233998347,-10.2967918855797));
#58928=CARTESIAN_POINT('Ctrl Pts',(-20.2388402640609,25.672288769313,-10.2907043858618));
#58929=CARTESIAN_POINT('Ctrl Pts',(-20.3014066280802,25.7699228349722,-10.2848525157784));
#58930=CARTESIAN_POINT('Ctrl Pts',(-20.3683241206917,25.8648335013899,-10.279000645695));
#58931=CARTESIAN_POINT('Ctrl Pts',(-20.4393198295186,25.956616328491,-10.2731487756116));
#58932=CARTESIAN_POINT('Ctrl Pts',(-20.5103047286033,26.0483851808221,-10.2672977965287));
#58933=CARTESIAN_POINT('Ctrl Pts',(-20.5853663564104,26.1370268138693,-10.2614468174457));
#58934=CARTESIAN_POINT('Ctrl Pts',(-20.6641901098758,26.2221680800167,-10.2555958383628));
#58935=CARTESIAN_POINT('Ctrl Pts',(-20.7430209503551,26.3073170011833,-10.2497443332205));
#58936=CARTESIAN_POINT('Ctrl Pts',(-20.8256143080533,26.388964626461,-10.2438928280782));
#58937=CARTESIAN_POINT('Ctrl Pts',(-20.9116176510668,26.4667735699753,-10.2380413229359));
#58938=CARTESIAN_POINT('Ctrl Pts',(-20.9976495539183,26.5446083521459,-10.2321878746362));
#58939=CARTESIAN_POINT('Ctrl Pts',(-21.0870933873727,26.6186016406174,-10.2263344263364));
#58940=CARTESIAN_POINT('Ctrl Pts',(-21.1795629412545,26.6884558179363,-10.2204809780366));
#58941=CARTESIAN_POINT('Ctrl Pts',(-21.2721376530984,26.7583894346234,-10.2146208730951));
#58942=CARTESIAN_POINT('Ctrl Pts',(-21.3677446232639,26.8241742956702,-10.2087607681536));
#58943=CARTESIAN_POINT('Ctrl Pts',(-21.4659679368872,26.8855556255449,-10.2029006632121));
#58944=CARTESIAN_POINT('Ctrl Pts',(-21.5642573977646,26.9469782919036,-10.1970366118566));
#58945=CARTESIAN_POINT('Ctrl Pts',(-21.6651663514486,27.0039913193353,-10.1911725605012));
#58946=CARTESIAN_POINT('Ctrl Pts',(-21.7682550763275,27.0563863096705,-10.1853085091458));
#58947=CARTESIAN_POINT('Ctrl Pts',(-21.8714957334084,27.1088585197625,-10.1794358153492));
#58948=CARTESIAN_POINT('Ctrl Pts',(-21.9769221982844,27.1566989389869,-10.1735631215527));
#58949=CARTESIAN_POINT('Ctrl Pts',(-22.0840755540415,27.199747574875,-10.1676904277561));
#58950=CARTESIAN_POINT('Ctrl Pts',(-22.1134123503931,27.2115335712662,-10.1660825824327));
#58951=CARTESIAN_POINT('Ctrl Pts',(-22.1428785094352,27.2229606791983,-10.1644747371092));
#58952=CARTESIAN_POINT('Ctrl Pts',(-22.1724644492979,27.2340262761045,-10.1628668917858));
#58953=CARTESIAN_POINT('Ctrl Pts',(-22.2805205057102,27.2744409044409,-10.1569945948171));
#58954=CARTESIAN_POINT('Ctrl Pts',(-22.390537315057,27.3101647982694,-10.1511222978484));
#58955=CARTESIAN_POINT('Ctrl Pts',(-22.5020699733967,27.3410047425992,-10.1452500008797));
#58956=CARTESIAN_POINT('Ctrl Pts',(-22.6134580942689,27.3718047208103,-10.1393853139414));
#58957=CARTESIAN_POINT('Ctrl Pts',(-22.7263577628541,27.3977332268973,-10.1335206270032));
#58958=CARTESIAN_POINT('Ctrl Pts',(-22.8403049898277,27.4186454134731,-10.127655940065));
#58959=CARTESIAN_POINT('Ctrl Pts',(-22.9541350292116,27.4395360931742,-10.1217972845902));
#58960=CARTESIAN_POINT('Ctrl Pts',(-23.0690100799351,27.4554206406507,-10.1159386291154));
#58961=CARTESIAN_POINT('Ctrl Pts',(-23.1844525598468,27.4662044441411,-10.1100799736406));
#58962=CARTESIAN_POINT('Ctrl Pts',(-23.3044043247042,27.4774094724941,-10.1039924739227));
#58963=CARTESIAN_POINT('Ctrl Pts',(-23.4249683127691,27.483107033148,-10.0979049742048));
#58964=CARTESIAN_POINT('Ctrl Pts',(-23.5455985110658,27.4832497780817,-10.0918174744869));
#58965=CARTESIAN_POINT('Ctrl Pts',(-23.6615594607623,27.483386997769,-10.0859656044035));
#58966=CARTESIAN_POINT('Ctrl Pts',(-23.7775811384447,27.4783914272242,-10.0801137343201));
#58967=CARTESIAN_POINT('Ctrl Pts',(-23.8931757611827,27.4682740552029,-10.0742618642367));
#58968=CARTESIAN_POINT('Ctrl Pts',(-24.0087527835882,27.4581582236435,-10.0684108851537));
#58969=CARTESIAN_POINT('Ctrl Pts',(-24.1239024686402,27.4429221772143,-10.0625599060707));
#58970=CARTESIAN_POINT('Ctrl Pts',(-24.2381408246955,27.4226288946465,-10.0567089269878));
#58971=CARTESIAN_POINT('Ctrl Pts',(-24.3523894518784,27.4023337875173,-10.0508574218455));
#58972=CARTESIAN_POINT('Ctrl Pts',(-24.4657261801457,27.3769806126651,-10.0450059167032));
#58973=CARTESIAN_POINT('Ctrl Pts',(-24.5776766026615,27.3466835897271,-10.0391544115609));
#58974=CARTESIAN_POINT('Ctrl Pts',(-24.6896642014754,27.3163765058074,-10.0333009632611));
#58975=CARTESIAN_POINT('Ctrl Pts',(-24.8002641803195,27.2811224172283,-10.0274475149614));
#58976=CARTESIAN_POINT('Ctrl Pts',(-24.9090173856644,27.2410853742401,-10.0215940666616));
#58977=CARTESIAN_POINT('Ctrl Pts',(-25.0178942670191,27.2010028004401,-10.0157339617201));
#58978=CARTESIAN_POINT('Ctrl Pts',(-25.1249197948141,27.1561265585363,-10.0098738567785));
#58979=CARTESIAN_POINT('Ctrl Pts',(-25.2296548025042,27.1066688477064,-10.004013751837));
#58980=CARTESIAN_POINT('Ctrl Pts',(-25.3344603426669,27.0571778302038,-9.99814970048156));
#58981=CARTESIAN_POINT('Ctrl Pts',(-25.4369719265244,27.0030993926744,-9.99228564912612));
#58982=CARTESIAN_POINT('Ctrl Pts',(-25.536776537028,26.944690832243,-9.98642159777068));
#58983=CARTESIAN_POINT('Ctrl Pts',(-25.6367282396045,26.886196189253,-9.98054890397411));
#58984=CARTESIAN_POINT('Ctrl Pts',(-25.733964660587,26.8233589101714,-9.97467621017755));
#58985=CARTESIAN_POINT('Ctrl Pts',(-25.8281031315803,26.756478606786,-9.96880351638099));
#58986=CARTESIAN_POINT('Ctrl Pts',(-25.8538766701948,26.7381678984893,-9.96719567105761));
#58987=CARTESIAN_POINT('Ctrl Pts',(-25.8794181959453,26.7195543607642,-9.96558782573423));
#58988=CARTESIAN_POINT('Ctrl Pts',(-25.9047203230156,26.7006446373899,-9.96397998041085));
#58989=CARTESIAN_POINT('Ctrl Pts',(-25.99620696118,26.6322714521903,-9.95816638367587));
#58990=CARTESIAN_POINT('Ctrl Pts',(-26.0848810300192,26.5597839066081,-9.95235278694089));
#58991=CARTESIAN_POINT('Ctrl Pts',(-26.1703438557641,26.4834437040411,-9.94653919020591));
#58992=CARTESIAN_POINT('Ctrl Pts',(-26.2556955458028,26.4072027741373,-9.94073315346175));
#58993=CARTESIAN_POINT('Ctrl Pts',(-26.3378439815586,26.3271194246759,-9.9349271167176));
#58994=CARTESIAN_POINT('Ctrl Pts',(-26.4164204716666,26.2434978491271,-9.92912107997345));
#58995=CARTESIAN_POINT('Ctrl Pts',(-26.4949168496792,26.1599615293543,-9.9233209627323));
#58996=CARTESIAN_POINT('Ctrl Pts',(-26.5698482352409,26.0728944618218,-9.91752084549115));
#58997=CARTESIAN_POINT('Ctrl Pts',(-26.6408805851238,25.9826396792005,-9.91172072825));
#58998=CARTESIAN_POINT('Ctrl Pts',(-26.7118616411519,25.8924500713302,-9.90592479938741));
#58999=CARTESIAN_POINT('Ctrl Pts',(-26.7789490000741,25.799077656742,-9.90012887052482));
#59000=CARTESIAN_POINT('Ctrl Pts',(-26.8418474637209,25.7029001580966,-9.89433294166223));
#59001=CARTESIAN_POINT('Ctrl Pts',(-26.9047224438966,25.6067585678247,-9.88853917674008));
#59002=CARTESIAN_POINT('Ctrl Pts',(-26.9634114058272,25.5078143278235,-9.88274541181792));
#59003=CARTESIAN_POINT('Ctrl Pts',(-27.0176616508371,25.4064753094028,-9.87695164689577));
#59004=CARTESIAN_POINT('Ctrl Pts',(-27.0719054207339,25.3051483864411,-9.87115857349646));
#59005=CARTESIAN_POINT('Ctrl Pts',(-27.1217113278621,25.201427625859,-9.86536550009714));
#59006=CARTESIAN_POINT('Ctrl Pts',(-27.1668723540204,25.0957460000586,-9.85957242669782));
#59007=CARTESIAN_POINT('Ctrl Pts',(-27.2120394611068,24.9900501442368,-9.85377857326169));
#59008=CARTESIAN_POINT('Ctrl Pts',(-27.252560279181,24.8823932873311,-9.84798471982556));
#59009=CARTESIAN_POINT('Ctrl Pts',(-27.2882760361925,24.7732281160042,-9.84219086638942));
#59010=CARTESIAN_POINT('Ctrl Pts',(-27.3240260308546,24.6639582973366,-9.83639145888007));
#59011=CARTESIAN_POINT('Ctrl Pts',(-27.3549616363811,24.5531776795425,-9.83059205137072));
#59012=CARTESIAN_POINT('Ctrl Pts',(-27.3809740699463,24.4413538145859,-9.82479264386136));
#59013=CARTESIAN_POINT('Ctrl Pts',(-27.4070000385292,24.3294717644551,-9.81899021875343));
#59014=CARTESIAN_POINT('Ctrl Pts',(-27.4280976577133,24.2165458013837,-9.81318779364549));
#59015=CARTESIAN_POINT('Ctrl Pts',(-27.4442096767031,24.1030515483667,-9.80738536853755));
#59016=CARTESIAN_POINT('Ctrl Pts',(-27.4603455593391,23.9893891980616,-9.80157434940922));
#59017=CARTESIAN_POINT('Ctrl Pts',(-27.4714810570642,23.8751572971363,-9.79576333028089));
#59018=CARTESIAN_POINT('Ctrl Pts',(-27.4776109559515,23.7608345998186,-9.78995231115256));
#59019=CARTESIAN_POINT('Ctrl Pts',(-27.4814045639771,23.6900837587301,-9.7863560481133));
#59020=CARTESIAN_POINT('Ctrl Pts',(-27.4832820636393,23.6192981373075,-9.78275978507405));
#59021=CARTESIAN_POINT('Ctrl Pts',(-27.4832521804468,23.5485903307078,-9.7791635220348));
#59022=CARTESIAN_POINT('',(-27.4839897010956,23.5538383238888,-8.5291635220348));
#59023=CARTESIAN_POINT('Ctrl Pts',(-27.4889022247121,23.5485879428334,-9.7791635220348));
#59024=CARTESIAN_POINT('Ctrl Pts',(-27.4893933224062,23.456239996285,-9.77447337103519));
#59025=CARTESIAN_POINT('Ctrl Pts',(-27.4445143940911,22.059032543948,-9.70348758291055));
#59026=CARTESIAN_POINT('Ctrl Pts',(-25.7819745911596,19.4685656890507,-9.56620615766113));
#59027=CARTESIAN_POINT('Ctrl Pts',(-21.3226012899819,19.4663425452466,-9.36731924628616));
#59028=CARTESIAN_POINT('Ctrl Pts',(-18.9102506062613,23.21688642052,-9.16843233491138));
#59029=CARTESIAN_POINT('Ctrl Pts',(-20.7616682847246,27.27376548718,-8.96954542353633));
#59030=CARTESIAN_POINT('Ctrl Pts',(-25.1755584532003,27.9090518495824,-8.77065851216153));
#59031=CARTESIAN_POINT('Ctrl Pts',(-27.3310193809219,25.4216709344377,-8.62386454499429));
#59032=CARTESIAN_POINT('Ctrl Pts',(-27.4865993094704,23.8343954513882,-8.54336621495207));
#59033=CARTESIAN_POINT('Ctrl Pts',(-27.4839897010956,23.5538383238888,-8.5291635220348));
#59034=CARTESIAN_POINT('',(-27.4767287689123,23.5502697193127,-7.2791635220348));
#59035=CARTESIAN_POINT('Ctrl Pts',(-27.4839897010956,23.5538383238888,-8.5291635220348));
#59036=CARTESIAN_POINT('Ctrl Pts',(-27.4744181230669,22.5248048247472,-8.47707057782711));
#59037=CARTESIAN_POINT('Ctrl Pts',(-26.5336429110486,20.1706869477114,-8.35868199649442));
#59038=CARTESIAN_POINT('Ctrl Pts',(-22.560216303688,19.0048615584841,-8.17399777803684));
#59039=CARTESIAN_POINT('Ctrl Pts',(-19.1909822903886,21.9262101075659,-7.97511086666202));
#59040=CARTESIAN_POINT('Ctrl Pts',(-19.8275480236813,26.3399159483343,-7.77622395528699));
#59041=CARTESIAN_POINT('Ctrl Pts',(-23.8849635665489,28.1901576336603,-7.57733704391218));
#59042=CARTESIAN_POINT('Ctrl Pts',(-27.0088482393263,26.1795939710675,-7.4116502328281));
#59043=CARTESIAN_POINT('Ctrl Pts',(-27.476754263685,24.207090521581,-7.31225905886896));
#59044=CARTESIAN_POINT('Ctrl Pts',(-27.4767287689123,23.5502697193127,-7.2791635220348));
#59045=CARTESIAN_POINT('',(-27.4839264031395,23.5466608562294,-6.02916352203481));
#59046=CARTESIAN_POINT('Ctrl Pts',(-27.4767287689123,23.5502697193127,-7.2791635220348));
#59047=CARTESIAN_POINT('Ctrl Pts',(-27.4767031935903,22.8913737292682,-7.245963421744));
#59048=CARTESIAN_POINT('Ctrl Pts',(-27.0066715029592,20.9167266579016,-7.14646768432824));
#59049=CARTESIAN_POINT('Ctrl Pts',(-23.8776470449471,18.909825432299,-6.9806763097875));
#59050=CARTESIAN_POINT('Ctrl Pts',(-19.8231539683923,20.7664624656976,-6.78178939841262));
#59051=CARTESIAN_POINT('Ctrl Pts',(-19.1935484656661,25.1811665432707,-6.58290248703777));
#59052=CARTESIAN_POINT('Ctrl Pts',(-22.5673846120303,28.0971989229123,-6.38401557566277));
#59053=CARTESIAN_POINT('Ctrl Pts',(-26.5367194223868,26.9257733735504,-6.19943592066184));
#59054=CARTESIAN_POINT('Ctrl Pts',(-27.4743736257135,24.5736712048814,-6.08115190278585));
#59055=CARTESIAN_POINT('Ctrl Pts',(-27.4839264031395,23.5466608562294,-6.02916352203481));
#59056=CARTESIAN_POINT('',(-27.4847663727323,23.5518813974934,-4.77916352203479));
#59057=CARTESIAN_POINT('Ctrl Pts',(-27.4839264031395,23.5466608562294,-6.02916352203481));
#59058=CARTESIAN_POINT('Ctrl Pts',(-27.486555337408,23.2640265417046,-6.01485626566089));
#59059=CARTESIAN_POINT('Ctrl Pts',(-27.3296020251925,21.674644395198,-5.93425337216194));
#59060=CARTESIAN_POINT('Ctrl Pts',(-25.1686835689709,19.1888958838517,-5.78735484153822));
#59061=CARTESIAN_POINT('Ctrl Pts',(-20.7558005937558,19.8311411864055,-5.58846793016332));
#59062=CARTESIAN_POINT('Ctrl Pts',(-18.9107820190502,23.8909344866399,-5.38958101878834));
#59063=CARTESIAN_POINT('Ctrl Pts',(-21.3290434832377,27.6376699553445,-5.19069410741347));
#59064=CARTESIAN_POINT('Ctrl Pts',(-25.788407735483,27.6284153675624,-4.99180719603861));
#59065=CARTESIAN_POINT('Ctrl Pts',(-27.4455976798272,25.0373053559045,-4.85463033424573));
#59066=CARTESIAN_POINT('Ctrl Pts',(-27.4894091699444,23.6421701040578,-4.78374910957776));
#59067=CARTESIAN_POINT('Ctrl Pts',(-27.4889373831764,23.5518831242674,-4.77916352203479));
#59068=CARTESIAN_POINT('',(-27.4824137648665,23.5530535657996,-3.52916356170341));
#59069=CARTESIAN_POINT('Ctrl Pts',(-27.4832521946535,23.5518807706325,-4.77916352203479));
#59070=CARTESIAN_POINT('Ctrl Pts',(-27.4832995073027,23.4375974003668,-4.77335077744995));
#59071=CARTESIAN_POINT('Ctrl Pts',(-27.4783614066125,23.3231104330131,-4.7675380328651));
#59072=CARTESIAN_POINT('Ctrl Pts',(-27.4684108958793,23.208896364083,-4.76172528828025));
#59073=CARTESIAN_POINT('Ctrl Pts',(-27.458472701503,23.0948236649049,-4.75591973848558));
#59074=CARTESIAN_POINT('Ctrl Pts',(-27.4435344664143,22.9810236096023,-4.7501141886909));
#59075=CARTESIAN_POINT('Ctrl Pts',(-27.4236211929847,22.8679738395655,-4.74430863889623));
#59076=CARTESIAN_POINT('Ctrl Pts',(-27.4037269798246,22.7550322767053,-4.73850864596515));
#59077=CARTESIAN_POINT('Ctrl Pts',(-27.3788672694762,22.6428399848093,-4.73270865303407));
#59078=CARTESIAN_POINT('Ctrl Pts',(-27.3491188987623,22.5318698309578,-4.726908660103));
#59079=CARTESIAN_POINT('Ctrl Pts',(-27.3193892046031,22.4209693461372,-4.72111230851035));
#59080=CARTESIAN_POINT('Ctrl Pts',(-27.2847770608197,22.3112898807109,-4.71531595691771));
#59081=CARTESIAN_POINT('Ctrl Pts',(-27.2454103083026,22.2032937327808,-4.70951960532507));
#59082=CARTESIAN_POINT('Ctrl Pts',(-27.2060559748648,22.0953316545322,-4.70372508231481));
#59083=CARTESIAN_POINT('Ctrl Pts',(-27.1619501578594,21.9890522349221,-4.69793055930455));
#59084=CARTESIAN_POINT('Ctrl Pts',(-27.1132702123033,21.8849015153416,-4.69213603629429));
#59085=CARTESIAN_POINT('Ctrl Pts',(-27.0645932674965,21.7807572158625,-4.68634187047239));
#59086=CARTESIAN_POINT('Ctrl Pts',(-27.011342933768,21.6787417380542,-4.68054770465049));
#59087=CARTESIAN_POINT('Ctrl Pts',(-26.9537439098953,21.579279310539,-4.67475353882859));
#59088=CARTESIAN_POINT('Ctrl Pts',(-26.896133815525,21.4797977664054,-4.66895825937153));
#59089=CARTESIAN_POINT('Ctrl Pts',(-26.8341735820922,21.3828706129,-4.66316297991446));
#59090=CARTESIAN_POINT('Ctrl Pts',(-26.7681324437633,21.2888950032387,-4.6573677004574));
#59091=CARTESIAN_POINT('Ctrl Pts',(-26.7020219864012,21.1948207535695,-4.6515663380772));
#59092=CARTESIAN_POINT('Ctrl Pts',(-26.6318223156162,21.1037045788478,-4.64576497569699));
#59093=CARTESIAN_POINT('Ctrl Pts',(-26.5578443679754,21.0159123125573,-4.63996361331678));
#59094=CARTESIAN_POINT('Ctrl Pts',(-26.4838243075402,20.9280700695132,-4.63415894844457));
#59095=CARTESIAN_POINT('Ctrl Pts',(-26.4060219746012,20.8435558116978,-4.62835428357235));
#59096=CARTESIAN_POINT('Ctrl Pts',(-26.3247854260627,20.7626987262821,-4.62254961870013));
#59097=CARTESIAN_POINT('Ctrl Pts',(-26.2434216288695,20.6817149866016,-4.61673586142051));
#59098=CARTESIAN_POINT('Ctrl Pts',(-26.1586131871594,20.6044001411639,-4.61092210414089));
#59099=CARTESIAN_POINT('Ctrl Pts',(-26.0707416448313,20.5310434248986,-4.60510834686127));
#59100=CARTESIAN_POINT('Ctrl Pts',(-26.014944394605,20.4844628944472,-4.60141668900378));
#59101=CARTESIAN_POINT('Ctrl Pts',(-25.9579127026491,20.4394774646879,-4.59772503114629));
#59102=CARTESIAN_POINT('Ctrl Pts',(-25.8997499236222,20.3961518666356,-4.5940333732888));
#59103=CARTESIAN_POINT('Ctrl Pts',(-25.8072307563115,20.3272341099171,-4.58816107632009));
#59104=CARTESIAN_POINT('Ctrl Pts',(-25.7115216787875,20.2622751428022,-4.58228877935138));
#59105=CARTESIAN_POINT('Ctrl Pts',(-25.6129961542005,20.201584475913,-4.57641648238267));
#59106=CARTESIAN_POINT('Ctrl Pts',(-25.5145983108687,20.1409724593082,-4.57055179544447));
#59107=CARTESIAN_POINT('Ctrl Pts',(-25.4133916275155,20.0846179578096,-4.56468710850628));
#59108=CARTESIAN_POINT('Ctrl Pts',(-25.3097813717287,20.0327893462313,-4.55882242156808));
#59109=CARTESIAN_POINT('Ctrl Pts',(-25.2062776726035,19.9810140371353,-4.55296376609324));
#59110=CARTESIAN_POINT('Ctrl Pts',(-25.1003756853129,19.9337555435576,-4.54710511061841));
#59111=CARTESIAN_POINT('Ctrl Pts',(-24.9925077271812,19.8912377802767,-4.54124645514357));
#59112=CARTESIAN_POINT('Ctrl Pts',(-24.8804263515962,19.847059235713,-4.53515895542567));
#59113=CARTESIAN_POINT('Ctrl Pts',(-24.7662226761918,19.8079995641882,-4.52907145570777));
#59114=CARTESIAN_POINT('Ctrl Pts',(-24.6504079070978,19.7742563518801,-4.52298395598987));
#59115=CARTESIAN_POINT('Ctrl Pts',(-24.5390759951661,19.7418192424306,-4.51713208590647));
#59116=CARTESIAN_POINT('Ctrl Pts',(-24.4262558259643,19.7142948016807,-4.51128021582307));
#59117=CARTESIAN_POINT('Ctrl Pts',(-24.3124189327844,19.6918083663538,-4.50542834573966));
#59118=CARTESIAN_POINT('Ctrl Pts',(-24.1985993723066,19.6693253547912,-4.4995773666567));
#59119=CARTESIAN_POINT('Ctrl Pts',(-24.0837638010889,19.6518789035333,-4.49372638757373));
#59120=CARTESIAN_POINT('Ctrl Pts',(-23.968394595011,19.6395433613665,-4.48787540849076));
#59121=CARTESIAN_POINT('Ctrl Pts',(-23.853015016131,19.6272067101157,-4.48202390334846));
#59122=CARTESIAN_POINT('Ctrl Pts',(-23.7371021180777,19.6199819253913,-4.47617239820615));
#59123=CARTESIAN_POINT('Ctrl Pts',(-23.6211433464772,19.617891473452,-4.47032089306385));
#59124=CARTESIAN_POINT('Ctrl Pts',(-23.5051460674937,19.6158003273192,-4.4644674447641));
#59125=CARTESIAN_POINT('Ctrl Pts',(-23.389103297769,19.6188469117042,-4.45861399646435));
#59126=CARTESIAN_POINT('Ctrl Pts',(-23.2735017156984,19.6270015856234,-4.4527605481646));
#59127=CARTESIAN_POINT('Ctrl Pts',(-23.157768669526,19.6351655331776,-4.44690044322306));
#59128=CARTESIAN_POINT('Ctrl Pts',(-23.0424782250408,19.6484491357631,-4.44104033828151));
#59129=CARTESIAN_POINT('Ctrl Pts',(-22.9281112786345,19.6667709415175,-4.43518023333997));
#59130=CARTESIAN_POINT('Ctrl Pts',(-22.8136673132476,19.6851050858613,-4.42931618198451));
#59131=CARTESIAN_POINT('Ctrl Pts',(-22.7001484881982,19.7084841061587,-4.42345213062905));
#59132=CARTESIAN_POINT('Ctrl Pts',(-22.5880231493654,19.7367759530611,-4.41758807927359));
#59133=CARTESIAN_POINT('Ctrl Pts',(-22.4757325601657,19.7651094964982,-4.41171538547702));
#59134=CARTESIAN_POINT('Ctrl Pts',(-22.3648399504818,19.7983701989171,-4.40584269168044));
#59135=CARTESIAN_POINT('Ctrl Pts',(-22.2557963073753,19.836376916744,-4.39996999788387));
#59136=CARTESIAN_POINT('Ctrl Pts',(-22.2259419819702,19.8467825203102,-4.39836215256054));
#59137=CARTESIAN_POINT('Ctrl Pts',(-22.1962261195809,19.8575436004932,-4.39675430723721));
#59138=CARTESIAN_POINT('Ctrl Pts',(-22.1666576645012,19.8686558341352,-4.39514646191389));
#59139=CARTESIAN_POINT('Ctrl Pts',(-22.0586654673578,19.9092407927657,-4.38927416494519));
#59140=CARTESIAN_POINT('Ctrl Pts',(-21.9522795846292,19.9546493699853,-4.3834018679765));
#59141=CARTESIAN_POINT('Ctrl Pts',(-21.8479622854598,20.0047346685922,-4.3775295710078));
#59142=CARTESIAN_POINT('Ctrl Pts',(-21.7437801732253,20.0547550606299,-4.37166488406961));
#59143=CARTESIAN_POINT('Ctrl Pts',(-21.6416616827766,20.1094399443087,-4.36580019713141));
#59144=CARTESIAN_POINT('Ctrl Pts',(-21.5420516666592,20.1685934291718,-4.35993551019322));
#59145=CARTESIAN_POINT('Ctrl Pts',(-21.442544093208,20.2276860783786,-4.35407685471841));
#59146=CARTESIAN_POINT('Ctrl Pts',(-21.3455402160124,20.291237977927,-4.34821819924361));
#59147=CARTESIAN_POINT('Ctrl Pts',(-21.2514621041735,20.3590064474288,-4.3423595437688));
#59148=CARTESIAN_POINT('Ctrl Pts',(-21.153709218423,20.4294220130393,-4.3362720440509));
#59149=CARTESIAN_POINT('Ctrl Pts',(-21.0591157334227,20.5043900729783,-4.33018454433299));
#59150=CARTESIAN_POINT('Ctrl Pts',(-20.9681242103239,20.5835873446571,-4.32409704461509));
#59151=CARTESIAN_POINT('Ctrl Pts',(-20.8806547078126,20.6597191173552,-4.31824517453171));
#59152=CARTESIAN_POINT('Ctrl Pts',(-20.796513849758,20.7397584915599,-4.31239330444832));
#59153=CARTESIAN_POINT('Ctrl Pts',(-20.7160619677825,20.8233765082135,-4.30654143436494));
#59154=CARTESIAN_POINT('Ctrl Pts',(-20.6356223353376,20.9069817932637,-4.30069045528199));
#59155=CARTESIAN_POINT('Ctrl Pts',(-20.558870848705,20.994164339556,-4.29483947619903));
#59156=CARTESIAN_POINT('Ctrl Pts',(-20.4861308033785,21.0845585048402,-4.28898849711608));
#59157=CARTESIAN_POINT('Ctrl Pts',(-20.413384218022,21.1749607974296,-4.28313699197381));
#59158=CARTESIAN_POINT('Ctrl Pts',(-20.34465005012,21.2685749609526,-4.27728548683155));
#59159=CARTESIAN_POINT('Ctrl Pts',(-20.2802106859383,21.3650030431906,-4.27143398168928));
#59160=CARTESIAN_POINT('Ctrl Pts',(-20.2157499228468,21.4614631470953,-4.26558053338955));
#59161=CARTESIAN_POINT('Ctrl Pts',(-20.1555870289678,21.5607386842724,-4.25972708508982));
#59162=CARTESIAN_POINT('Ctrl Pts',(-20.0999601371491,21.6624041818144,-4.25387363679009));
#59163=CARTESIAN_POINT('Ctrl Pts',(-20.0442699854748,21.7641852951039,-4.24801353184856));
#59164=CARTESIAN_POINT('Ctrl Pts',(-19.9931263304524,21.86836143075,-4.24215342690702));
#59165=CARTESIAN_POINT('Ctrl Pts',(-19.9467205901495,21.974483974365,-4.23629332196549));
#59166=CARTESIAN_POINT('Ctrl Pts',(-19.9002835984851,22.0806779848711,-4.23042927061004));
#59167=CARTESIAN_POINT('Ctrl Pts',(-19.8585910231763,22.1888206286094,-4.2245652192546));
#59168=CARTESIAN_POINT('Ctrl Pts',(-19.8217849296931,22.2984465000629,-4.21870116789916));
#59169=CARTESIAN_POINT('Ctrl Pts',(-19.7849245913754,22.4082339381675,-4.2128284741026));
#59170=CARTESIAN_POINT('Ctrl Pts',(-19.7529652217709,22.5195085709564,-4.20695578030604));
#59171=CARTESIAN_POINT('Ctrl Pts',(-19.7259981993774,22.6317930596673,-4.20108308650949));
#59172=CARTESIAN_POINT('Ctrl Pts',(-19.7186150797485,22.662534674389,-4.19947524118601));
#59173=CARTESIAN_POINT('Ctrl Pts',(-19.7116058736916,22.6933519480334,-4.19786739586254));
#59174=CARTESIAN_POINT('Ctrl Pts',(-19.7049717788315,22.724235018766,-4.19625955053907));
#59175=CARTESIAN_POINT('Ctrl Pts',(-19.6807422248015,22.8370285568011,-4.19038725357036));
#59176=CARTESIAN_POINT('Ctrl Pts',(-19.6614391430601,22.951078045903,-4.18451495660165));
#59177=CARTESIAN_POINT('Ctrl Pts',(-19.6471888225963,23.0659151671195,-4.17864265963295));
#59178=CARTESIAN_POINT('Ctrl Pts',(-19.6329569694161,23.180603468547,-4.17277797269474));
#59179=CARTESIAN_POINT('Ctrl Pts',(-19.623764906374,23.2960769658161,-4.16691328575654));
#59180=CARTESIAN_POINT('Ctrl Pts',(-19.6196882892013,23.4118555099198,-4.16104859881834));
#59181=CARTESIAN_POINT('Ctrl Pts',(-19.6156158645741,23.5275149830393,-4.15518994334349));
#59182=CARTESIAN_POINT('Ctrl Pts',(-19.6166484360432,23.6434784683419,-4.14933128786865));
#59183=CARTESIAN_POINT('Ctrl Pts',(-19.6228099787682,23.7592596929737,-4.1434726323938));
#59184=CARTESIAN_POINT('Ctrl Pts',(-19.629212196779,23.8795634342178,-4.1373851326759));
#59185=CARTESIAN_POINT('Ctrl Pts',(-19.6411522946933,23.99966993478,-4.131297632958));
#59186=CARTESIAN_POINT('Ctrl Pts',(-19.6585975125088,24.1190321125942,-4.1252101332401));
#59187=CARTESIAN_POINT('Ctrl Pts',(-19.6753674760346,24.2337741232403,-4.11935826315671));
#59188=CARTESIAN_POINT('Ctrl Pts',(-19.6972242437108,24.3478279137254,-4.11350639307332));
#59189=CARTESIAN_POINT('Ctrl Pts',(-19.7240858312803,24.4607125146937,-4.10765452298992));
#59190=CARTESIAN_POINT('Ctrl Pts',(-19.7509433289288,24.5735799279553,-4.10180354390695));
#59191=CARTESIAN_POINT('Ctrl Pts',(-19.7828040356436,24.6852781036165,-4.09595256482398));
#59192=CARTESIAN_POINT('Ctrl Pts',(-19.8195350853847,24.7953374026173,-4.09010158574101));
#59193=CARTESIAN_POINT('Ctrl Pts',(-19.8562694376005,24.9054065970081,-4.08425008059872));
#59194=CARTESIAN_POINT('Ctrl Pts',(-19.897874872455,25.0138362296735,-4.07839857545642));
#59195=CARTESIAN_POINT('Ctrl Pts',(-19.9441692278176,25.1201736142657,-4.07254707031413));
#59196=CARTESIAN_POINT('Ctrl Pts',(-19.9904789565281,25.2265463111891,-4.06669362201433));
#59197=CARTESIAN_POINT('Ctrl Pts',(-20.0414805369979,25.3308249996716,-4.06084017371453));
#59198=CARTESIAN_POINT('Ctrl Pts',(-20.0969447326303,25.4325793484093,-4.05498672541473));
#59199=CARTESIAN_POINT('Ctrl Pts',(-20.1524720030967,25.5344494139364,-4.0491266204732));
#59200=CARTESIAN_POINT('Ctrl Pts',(-20.2124718202358,25.633789046664,-4.04326651553167));
#59201=CARTESIAN_POINT('Ctrl Pts',(-20.2766702268169,25.7301947082655,-4.03740641059013));
#59202=CARTESIAN_POINT('Ctrl Pts',(-20.3409118670067,25.8266652930459,-4.03154235923471));
#59203=CARTESIAN_POINT('Ctrl Pts',(-20.4093574831997,25.9201976396138,-4.02567830787928));
#59204=CARTESIAN_POINT('Ctrl Pts',(-20.4816923143348,26.0104206544937,-4.01981425652385));
#59205=CARTESIAN_POINT('Ctrl Pts',(-20.5541337525718,26.1007766400877,-4.01394156272729));
#59206=CARTESIAN_POINT('Ctrl Pts',(-20.6304755740057,26.187813250247,-4.00806886893072));
#59207=CARTESIAN_POINT('Ctrl Pts',(-20.7103655794784,26.2711955848716,-4.00219617513415));
#59208=CARTESIAN_POINT('Ctrl Pts',(-20.7322381265803,26.2940242732758,-4.00058832981082));
#59209=CARTESIAN_POINT('Ctrl Pts',(-20.7543764429403,26.3165792787735,-3.99898048448748));
#59210=CARTESIAN_POINT('Ctrl Pts',(-20.7767728789984,26.3388542630432,-3.99737263916415));
#59211=CARTESIAN_POINT('Ctrl Pts',(-20.8585708739085,26.4202086823437,-3.99150034219543));
#59212=CARTESIAN_POINT('Ctrl Pts',(-20.9440884886437,26.4980972726453,-3.98562804522671));
#59213=CARTESIAN_POINT('Ctrl Pts',(-21.0329999831643,26.5721606386557,-3.97975574825799));
#59214=CARTESIAN_POINT('Ctrl Pts',(-21.1217962554489,26.6461280244254,-3.97389106131979));
#59215=CARTESIAN_POINT('Ctrl Pts',(-21.2139773463907,26.7162797818324,-3.96802637438158));
#59216=CARTESIAN_POINT('Ctrl Pts',(-21.3091801937043,26.7822927195472,-3.96216168744338));
#59217=CARTESIAN_POINT('Ctrl Pts',(-21.4042851308495,26.8482377670881,-3.95630303196855));
#59218=CARTESIAN_POINT('Ctrl Pts',(-21.5024053053512,26.9100522272334,-3.95044437649372));
#59219=CARTESIAN_POINT('Ctrl Pts',(-21.6031445672889,26.9674530781868,-3.94458572101889));
#59220=CARTESIAN_POINT('Ctrl Pts',(-21.7078187935275,27.0270960569363,-3.93849822130099));
#59221=CARTESIAN_POINT('Ctrl Pts',(-21.8153205367264,27.0819733074569,-3.93241072158309));
#59222=CARTESIAN_POINT('Ctrl Pts',(-21.9251718193941,27.131816670239,-3.92632322186519));
#59223=CARTESIAN_POINT('Ctrl Pts',(-22.0307710743358,27.1797307395676,-3.92047135178177));
#59224=CARTESIAN_POINT('Ctrl Pts',(-22.1385409513973,27.2229931830441,-3.91461948169836));
#59225=CARTESIAN_POINT('Ctrl Pts',(-22.2480324870229,27.2614129910729,-3.90876761161494));
#59226=CARTESIAN_POINT('Ctrl Pts',(-22.3575073515665,27.2998269493366,-3.90291663253196));
#59227=CARTESIAN_POINT('Ctrl Pts',(-22.4687029635005,27.3333996013773,-3.89706565344898));
#59228=CARTESIAN_POINT('Ctrl Pts',(-22.5811523878769,27.3619888698022,-3.891214674366));
#59229=CARTESIAN_POINT('Ctrl Pts',(-22.6936119225386,27.3905807086775,-3.8853631692237));
#59230=CARTESIAN_POINT('Ctrl Pts',(-22.8073250930779,27.4141881713822,-3.87951166408139));
#59231=CARTESIAN_POINT('Ctrl Pts',(-22.921812580521,27.4327198178113,-3.87366015893909));
#59232=CARTESIAN_POINT('Ctrl Pts',(-23.0363380867664,27.4512576181967,-3.8678067106393));
#59233=CARTESIAN_POINT('Ctrl Pts',(-23.1516380133544,27.4647161846424,-3.86195326233952));
#59234=CARTESIAN_POINT('Ctrl Pts',(-23.2672264032402,27.4730557654305,-3.85609981403973));
#59235=CARTESIAN_POINT('Ctrl Pts',(-23.3829462422248,27.4814048301329,-3.85023970909818));
#59236=CARTESIAN_POINT('Ctrl Pts',(-23.4989547867203,27.4846232600772,-3.84437960415663));
#59237=CARTESIAN_POINT('Ctrl Pts',(-23.6147644476646,27.4827234105054,-3.83851949921508));
#59238=CARTESIAN_POINT('Ctrl Pts',(-23.7306520991673,27.4808222815037,-3.83265544785962));
#59239=CARTESIAN_POINT('Ctrl Pts',(-23.8463401888123,27.4737960346405,-3.82679139650416));
#59240=CARTESIAN_POINT('Ctrl Pts',(-23.9613463677351,27.4617088919223,-3.8209273451487));
#59241=CARTESIAN_POINT('Ctrl Pts',(-24.0765220428081,27.4496039351687,-3.81505465135212));
#59242=CARTESIAN_POINT('Ctrl Pts',(-24.1910133941017,27.4324232574492,-3.80918195755554));
#59243=CARTESIAN_POINT('Ctrl Pts',(-24.3043482859667,27.4102821421231,-3.80330926375897));
#59244=CARTESIAN_POINT('Ctrl Pts',(-24.3353774834963,27.4042202751229,-3.80170141843573));
#59245=CARTESIAN_POINT('Ctrl Pts',(-24.3663200865554,27.3977868747735,-3.80009357311249));
#59246=CARTESIAN_POINT('Ctrl Pts',(-24.3971666276965,27.3909849506467,-3.79848572778926));
#59247=CARTESIAN_POINT('Ctrl Pts',(-24.5098267495501,27.3661424375926,-3.79261343082056));
#59248=CARTESIAN_POINT('Ctrl Pts',(-24.6215816235178,27.3362971184701,-3.78674113385187));
#59249=CARTESIAN_POINT('Ctrl Pts',(-24.7319528080094,27.3015287754486,-3.78086883688317));
#59250=CARTESIAN_POINT('Ctrl Pts',(-24.842180960212,27.2668054894384,-3.77500414994495));
#59251=CARTESIAN_POINT('Ctrl Pts',(-24.9510285982303,27.2271719898143,-3.76913946300673));
#59252=CARTESIAN_POINT('Ctrl Pts',(-25.0580275652196,27.1827590283543,-3.76327477606851));
#59253=CARTESIAN_POINT('Ctrl Pts',(-25.1649164904692,27.138391742845,-3.7574161205937));
#59254=CARTESIAN_POINT('Ctrl Pts',(-25.269960146855,27.0892549299618,-3.75155746511889));
#59255=CARTESIAN_POINT('Ctrl Pts',(-25.3727062875652,27.0355288920007,-3.74569880964408));
#59256=CARTESIAN_POINT('Ctrl Pts',(-25.4794657830293,26.9797042676756,-3.73961130992617));
#59257=CARTESIAN_POINT('Ctrl Pts',(-25.5837441841579,26.9189247277497,-3.73352381020827));
#59258=CARTESIAN_POINT('Ctrl Pts',(-25.6850575167591,26.8534474511233,-3.72743631049037));
#59259=CARTESIAN_POINT('Ctrl Pts',(-25.7824493011653,26.7905046118643,-3.72158444040697));
#59260=CARTESIAN_POINT('Ctrl Pts',(-25.8771009079708,26.7232211908274,-3.71573257032357));
#59261=CARTESIAN_POINT('Ctrl Pts',(-25.9686089537636,26.6518716598006,-3.70988070024017));
#59262=CARTESIAN_POINT('Ctrl Pts',(-26.0601030666242,26.5805329923888,-3.70402972115721));
#59263=CARTESIAN_POINT('Ctrl Pts',(-26.148454244243,26.5051297000753,-3.69817874207425));
#59264=CARTESIAN_POINT('Ctrl Pts',(-26.2332905563915,26.4259778242123,-3.69232776299129));
#59265=CARTESIAN_POINT('Ctrl Pts',(-26.318134496141,26.3468188318338,-3.68647625784899));
#59266=CARTESIAN_POINT('Ctrl Pts',(-26.3994626399264,26.2639108679347,-3.68062475270668));
#59267=CARTESIAN_POINT('Ctrl Pts',(-26.4769389654279,26.1776077643567,-3.67477324756437));
#59268=CARTESIAN_POINT('Ctrl Pts',(-26.5544410191304,26.0912760013968,-3.6689197992646));
#59269=CARTESIAN_POINT('Ctrl Pts',(-26.628088435124,26.0015471643409,-3.66306635096482));
#59270=CARTESIAN_POINT('Ctrl Pts',(-26.6975850892375,25.9088086095155,-3.65721290266504));
#59271=CARTESIAN_POINT('Ctrl Pts',(-26.7671607761376,25.8159645908156,-3.6513527977235));
#59272=CARTESIAN_POINT('Ctrl Pts',(-26.8325760315004,25.7201043537356,-3.64549269278197));
#59273=CARTESIAN_POINT('Ctrl Pts',(-26.8935776874398,25.6216447936664,-3.63963258784043));
#59274=CARTESIAN_POINT('Ctrl Pts',(-26.9546204241767,25.5231189272458,-3.63376853648498));
#59275=CARTESIAN_POINT('Ctrl Pts',(-27.0112434416218,25.4219906120911,-3.62790448512954));
#59276=CARTESIAN_POINT('Ctrl Pts',(-27.0632400408178,25.318700371112,-3.62204043377409));
#59277=CARTESIAN_POINT('Ctrl Pts',(-27.1153132726214,25.2152579009365,-3.61616773997752));
#59278=CARTESIAN_POINT('Ctrl Pts',(-27.1627463092014,25.1096475214814,-3.61029504618096));
#59279=CARTESIAN_POINT('Ctrl Pts',(-27.2053809310488,25.0023287639327,-3.6044223523844));
#59280=CARTESIAN_POINT('Ctrl Pts',(-27.2170535773205,24.9729466833391,-3.60281450706105));
#59281=CARTESIAN_POINT('Ctrl Pts',(-27.2283668383697,24.9434366266009,-3.60120666173771));
#59282=CARTESIAN_POINT('Ctrl Pts',(-27.2393181286426,24.9138081856414,-3.59959881641437));
#59283=CARTESIAN_POINT('Ctrl Pts',(-27.2854146357158,24.7890952427623,-3.59283102454024));
#59284=CARTESIAN_POINT('Ctrl Pts',(-27.3252216568937,24.6619388292607,-3.58606323266611));
#59285=CARTESIAN_POINT('Ctrl Pts',(-27.3585091715111,24.532937814626,-3.57929544079198));
#59286=CARTESIAN_POINT('Ctrl Pts',(-27.3916624030074,24.4044571950725,-3.57255495045197));
#59287=CARTESIAN_POINT('Ctrl Pts',(-27.4183485169574,24.2741469668576,-3.56581446011196));
#59288=CARTESIAN_POINT('Ctrl Pts',(-27.438386915938,24.142620668971,-3.55907396977195));
#59289=CARTESIAN_POINT('Ctrl Pts',(-27.4582772032158,24.0120665337798,-3.55238330105211));
#59290=CARTESIAN_POINT('Ctrl Pts',(-27.4716175947566,23.880314395183,-3.54569263233228));
#59291=CARTESIAN_POINT('Ctrl Pts',(-27.4782789309084,23.7479836801672,-3.53900196361245));
#59292=CARTESIAN_POINT('Ctrl Pts',(-27.4815440175391,23.6831211302845,-3.53572249947944));
#59293=CARTESIAN_POINT('Ctrl Pts',(-27.4832051818487,23.6181198580839,-3.53244303534644));
#59294=CARTESIAN_POINT('Ctrl Pts',(-27.4832515337037,23.5530543510895,-3.52916357121343));
#59295=CARTESIAN_POINT('',(-27.4787306259862,23.5475518707578,-2.27916352203481));
#59296=CARTESIAN_POINT('Ctrl Pts',(-27.4789192294965,23.5530502901666,-3.52916352203482));
#59297=CARTESIAN_POINT('Ctrl Pts',(-27.4733707979894,22.7044760387893,-3.48634631636971));
#59298=CARTESIAN_POINT('Ctrl Pts',(-26.7862294952183,20.5338307647598,-3.37723347357964));
#59299=CARTESIAN_POINT('Ctrl Pts',(-23.2036002208863,18.9112242921254,-3.20182499366464));
#59300=CARTESIAN_POINT('Ctrl Pts',(-19.4599799693547,21.3343055111431,-3.00293808228964));
#59301=CARTESIAN_POINT('Ctrl Pts',(-19.4749734046927,25.7936541607236,-2.8040511709148));
#59302=CARTESIAN_POINT('Ctrl Pts',(-23.2348028310531,28.1915069223165,-2.60516425953992));
#59303=CARTESIAN_POINT('Ctrl Pts',(-26.7973600627289,26.5490322383971,-2.4302017099133));
#59304=CARTESIAN_POINT('Ctrl Pts',(-27.4734464956764,24.3873896537201,-2.32153479741155));
#59305=CARTESIAN_POINT('Ctrl Pts',(-27.4787306259862,23.5475518707578,-2.27916352203481));
#59306=CARTESIAN_POINT('',(-27.4887831525091,23.5484783899485,-1.02916352203483));
#59307=CARTESIAN_POINT('Ctrl Pts',(-27.4787306259862,23.5475518707578,-2.27916352203481));
#59308=CARTESIAN_POINT('Ctrl Pts',(-27.4817142379717,23.0733489408066,-2.25523916028659));
#59309=CARTESIAN_POINT('Ctrl Pts',(-27.1823788944945,21.2887449913975,-2.16501916141351));
#59310=CARTESIAN_POINT('Ctrl Pts',(-24.5214140722119,19.0007914543429,-2.00850352541525));
#59311=CARTESIAN_POINT('Ctrl Pts',(-20.2476685784447,20.2740214556172,-1.80961661404031));
#59312=CARTESIAN_POINT('Ctrl Pts',(-19.0087177247742,24.5578300372182,-1.61072970266545));
#59313=CARTESIAN_POINT('Ctrl Pts',(-21.9430523000085,27.9157603197271,-1.41184279129057));
#59314=CARTESIAN_POINT('Ctrl Pts',(-26.2426709926684,27.278694135458,-1.21798739774704));
#59315=CARTESIAN_POINT('Ctrl Pts',(-27.4820131566245,24.7548508141379,-1.09042764132844));
#59316=CARTESIAN_POINT('Ctrl Pts',(-27.4887831525091,23.5484783899485,-1.02916352203483));
#59317=CARTESIAN_POINT('',(-27.4832509175595,23.553815786008,0.220836477965203));
#59318=CARTESIAN_POINT('Ctrl Pts',(-27.4887831525091,23.5484783899485,-1.02916352203483));
#59319=CARTESIAN_POINT('Ctrl Pts',(-27.4893391607469,23.4494010762854,-1.02413200420349));
#59320=CARTESIAN_POINT('Ctrl Pts',(-27.4409537024358,22.045426077291,-0.952804849247351));
#59321=CARTESIAN_POINT('Ctrl Pts',(-25.7609338543555,19.4571316048489,-0.815182057165814));
#59322=CARTESIAN_POINT('Ctrl Pts',(-21.3016081928786,19.477863862914,-0.616295145791017));
#59323=CARTESIAN_POINT('Ctrl Pts',(-18.9085960251757,23.2407760259621,-0.417408234416091));
#59324=CARTESIAN_POINT('Ctrl Pts',(-20.7808726393893,27.2880708585003,-0.21852132304123));
#59325=CARTESIAN_POINT('Ctrl Pts',(-25.1979745699378,27.9006275634348,-0.0196344116663155));
#59326=CARTESIAN_POINT('Ctrl Pts',(-27.3356200838471,25.4079940948567,0.126818188669141));
#59327=CARTESIAN_POINT('Ctrl Pts',(-27.4867411403313,23.8275935976074,0.206975151879653));
#59328=CARTESIAN_POINT('Ctrl Pts',(-27.4841962167909,23.553816642439,0.220836477965203));
#59329=CARTESIAN_POINT('',(-27.4832525295589,23.5503821330865,1.47083647793937));
#59330=CARTESIAN_POINT('Ctrl Pts',(-27.4832509175595,23.553815786008,0.220836477965203));
#59331=CARTESIAN_POINT('Ctrl Pts',(-27.4833542858497,23.4397213984313,0.226614518140672));
#59332=CARTESIAN_POINT('Ctrl Pts',(-27.4784887302081,23.3254706986072,0.232392558316141));
#59333=CARTESIAN_POINT('Ctrl Pts',(-27.4686401989256,23.2115386564409,0.23817059849161));
#59334=CARTESIAN_POINT('Ctrl Pts',(-27.4586996367026,23.0965419608061,0.244002632349603));
#59335=CARTESIAN_POINT('Ctrl Pts',(-27.4436824350315,22.9818703461215,0.249834666207596));
#59336=CARTESIAN_POINT('Ctrl Pts',(-27.4236280539117,22.8680127909239,0.255666700065589));
#59337=CARTESIAN_POINT('Ctrl Pts',(-27.4037855365418,22.7553580795567,0.261437121622734));
#59338=CARTESIAN_POINT('Ctrl Pts',(-27.3790118409753,22.6435007384169,0.26720754317988));
#59339=CARTESIAN_POINT('Ctrl Pts',(-27.3493971970699,22.5329085330647,0.272977964737026));
#59340=CARTESIAN_POINT('Ctrl Pts',(-27.319788509928,22.4223385725053,0.278747225617147));
#59341=CARTESIAN_POINT('Ctrl Pts',(-27.2853409196067,22.3130336535003,0.284516486497268));
#59342=CARTESIAN_POINT('Ctrl Pts',(-27.2461952705643,22.2054490995922,0.290285747377388));
#59343=CARTESIAN_POINT('Ctrl Pts',(-27.2070473908893,22.0978584152042,0.296055337006728));
#59344=CARTESIAN_POINT('Ctrl Pts',(-27.1632010670632,21.9919886908855,0.301824926636067));
#59345=CARTESIAN_POINT('Ctrl Pts',(-27.1148459892455,21.8882770558276,0.307594516265406));
#59346=CARTESIAN_POINT('Ctrl Pts',(-27.0655761090386,21.7826033589589,0.313473257500241));
#59347=CARTESIAN_POINT('Ctrl Pts',(-27.0116253273253,21.6791706589197,0.319351998735076));
#59348=CARTESIAN_POINT('Ctrl Pts',(-26.9532435959297,21.5784156173595,0.32523073996991));
#59349=CARTESIAN_POINT('Ctrl Pts',(-26.8958639473396,21.4793899677219,0.33100857660038));
#59350=CARTESIAN_POINT('Ctrl Pts',(-26.8342045364938,21.3829511128856,0.336786413230851));
#59351=CARTESIAN_POINT('Ctrl Pts',(-26.7685460230031,21.289483635102,0.34256424986132));
#59352=CARTESIAN_POINT('Ctrl Pts',(-26.701167511159,21.193567671976,0.348493443398336));
#59353=CARTESIAN_POINT('Ctrl Pts',(-26.6295777721164,21.1007813005844,0.354422636935352));
#59354=CARTESIAN_POINT('Ctrl Pts',(-26.5541226147364,21.0115021453419,0.360351830472368));
#59355=CARTESIAN_POINT('Ctrl Pts',(-26.4786674573564,20.9222229900995,0.366281024009383));
#59356=CARTESIAN_POINT('Ctrl Pts',(-26.3993472589769,20.8364513510652,0.372210217546399));
#59357=CARTESIAN_POINT('Ctrl Pts',(-26.3165455762268,20.7545215375228,0.378139411083413));
#59358=CARTESIAN_POINT('Ctrl Pts',(-26.234538458803,20.6733779228458,0.384011708052126));
#59359=CARTESIAN_POINT('Ctrl Pts',(-26.1488206543725,20.5957096994031,0.389884005020839));
#59360=CARTESIAN_POINT('Ctrl Pts',(-26.0597188269229,20.521875422893,0.395756301989552));
#59361=CARTESIAN_POINT('Ctrl Pts',(-25.9707324683655,20.4481368297416,0.401620988927755));
#59362=CARTESIAN_POINT('Ctrl Pts',(-25.8783711231886,20.3782225643042,0.407485675865959));
#59363=CARTESIAN_POINT('Ctrl Pts',(-25.7829986843189,20.3124548823746,0.413350362804161));
#59364=CARTESIAN_POINT('Ctrl Pts',(-25.6877243300318,20.2467548383885,0.419209018279003));
#59365=CARTESIAN_POINT('Ctrl Pts',(-25.5894453798566,20.185193128862,0.425067673753843));
#59366=CARTESIAN_POINT('Ctrl Pts',(-25.4885587108555,20.1280517550265,0.430926329228684));
#59367=CARTESIAN_POINT('Ctrl Pts',(-25.3837313197037,20.0686783887996,0.437013828946586));
#59368=CARTESIAN_POINT('Ctrl Pts',(-25.276088687191,20.0140780125991,0.443101328664488));
#59369=CARTESIAN_POINT('Ctrl Pts',(-25.1661094794257,19.9645175548076,0.44918882838239));
#59370=CARTESIAN_POINT('Ctrl Pts',(-25.0603872509999,19.9168754400298,0.455040698465796));
#59371=CARTESIAN_POINT('Ctrl Pts',(-24.9525063801961,19.8738905225357,0.460892568549203));
#59372=CARTESIAN_POINT('Ctrl Pts',(-24.8429163207115,19.8357526557266,0.466744438632609));
#59373=CARTESIAN_POINT('Ctrl Pts',(-24.7333429473099,19.7976205957545,0.472595417715589));
#59374=CARTESIAN_POINT('Ctrl Pts',(-24.6220612929769,19.764334254902,0.478446396798569));
#59375=CARTESIAN_POINT('Ctrl Pts',(-24.5095386567988,19.7360345082742,0.484297375881548));
#59376=CARTESIAN_POINT('Ctrl Pts',(-24.3970059037529,19.7077322172269,0.490148881023854));
#59377=CARTESIAN_POINT('Ctrl Pts',(-24.2832323479808,19.6844175125015,0.49600038616616));
#59378=CARTESIAN_POINT('Ctrl Pts',(-24.168697542221,19.6661806002086,0.501851891308466));
#59379=CARTESIAN_POINT('Ctrl Pts',(-24.0541247019454,19.6479376318341,0.507705339608255));
#59380=CARTESIAN_POINT('Ctrl Pts',(-23.9387905170403,19.6347758738111,0.513558787908044));
#59381=CARTESIAN_POINT('Ctrl Pts',(-23.8231810452553,19.626733826949,0.519412236207833));
#59382=CARTESIAN_POINT('Ctrl Pts',(-23.7074401003969,19.6186826345334,0.525272341149383));
#59383=CARTESIAN_POINT('Ctrl Pts',(-23.5914236564294,19.6157628029639,0.531132446090934));
#59384=CARTESIAN_POINT('Ctrl Pts',(-23.4756192689992,19.6179607220621,0.536992551032484));
#59385=CARTESIAN_POINT('Ctrl Pts',(-23.3597368945622,19.6201601213213,0.542856602387933));
#59386=CARTESIAN_POINT('Ctrl Pts',(-23.2440672725678,19.6274841078253,0.548720653743383));
#59387=CARTESIAN_POINT('Ctrl Pts',(-23.1290925849853,19.6398672182899,0.554584705098832));
#59388=CARTESIAN_POINT('Ctrl Pts',(-23.0139484476643,19.6522685789874,0.56045739889541));
#59389=CARTESIAN_POINT('Ctrl Pts',(-22.8995016959622,19.6697438824968,0.566330092691988));
#59390=CARTESIAN_POINT('Ctrl Pts',(-22.7862241672427,19.6921766306376,0.572202786488567));
#59391=CARTESIAN_POINT('Ctrl Pts',(-22.7552106747825,19.6983183418242,0.573810631811822));
#59392=CARTESIAN_POINT('Ctrl Pts',(-22.7242847327741,19.7048313622487,0.575418477135078));
#59393=CARTESIAN_POINT('Ctrl Pts',(-22.6934558008877,19.7117126579819,0.577026322458334));
#59394=CARTESIAN_POINT('Ctrl Pts',(-22.5808599929164,19.7368450581513,0.582898619427047));
#59395=CARTESIAN_POINT('Ctrl Pts',(-22.4691823062669,19.7669779178527,0.58877091639576));
#59396=CARTESIAN_POINT('Ctrl Pts',(-22.3589009755982,19.8020302237477,0.594643213364473));
#59397=CARTESIAN_POINT('Ctrl Pts',(-22.2487625607758,19.837037104638,0.600507900302673));
#59398=CARTESIAN_POINT('Ctrl Pts',(-22.1400172936811,19.8769506296518,0.606372587240873));
#59399=CARTESIAN_POINT('Ctrl Pts',(-22.0331329930736,19.9216388424824,0.612237274179074));
#59400=CARTESIAN_POINT('Ctrl Pts',(-21.9263586162782,19.9662810962835,0.61809592965389));
#59401=CARTESIAN_POINT('Ctrl Pts',(-21.8214417782464,20.0156881122291,0.623954585128706));
#59402=CARTESIAN_POINT('Ctrl Pts',(-21.7188342602223,20.069678424608,0.629813240603522));
#59403=CARTESIAN_POINT('Ctrl Pts',(-21.6122188021685,20.1257776461426,0.635900740321426));
#59404=CARTESIAN_POINT('Ctrl Pts',(-21.5080971834041,20.1868253809196,0.64198824003933));
#59405=CARTESIAN_POINT('Ctrl Pts',(-21.4069527145798,20.2525632052176,0.648075739757234));
#59406=CARTESIAN_POINT('Ctrl Pts',(-21.3097232577186,20.3157565070959,0.65392760984064));
#59407=CARTESIAN_POINT('Ctrl Pts',(-21.215245141355,20.3832833235894,0.659779479924045));
#59408=CARTESIAN_POINT('Ctrl Pts',(-21.1239210411182,20.4548681455736,0.665631350007451));
#59409=CARTESIAN_POINT('Ctrl Pts',(-21.0326108458059,20.5264420681178,0.67148232909043));
#59410=CARTESIAN_POINT('Ctrl Pts',(-20.9444540370291,20.6020725126803,0.677333308173409));
#59411=CARTESIAN_POINT('Ctrl Pts',(-20.8598217303437,20.6814424816657,0.683184287256388));
#59412=CARTESIAN_POINT('Ctrl Pts',(-20.7751818143996,20.760819586775,0.689035792398682));
#59413=CARTESIAN_POINT('Ctrl Pts',(-20.6940673320361,20.8439366018822,0.694887297540977));
#59414=CARTESIAN_POINT('Ctrl Pts',(-20.6168133937526,20.930438831449,0.700738802683271));
#59415=CARTESIAN_POINT('Ctrl Pts',(-20.5395338011181,21.016969786523,0.706592250983026));
#59416=CARTESIAN_POINT('Ctrl Pts',(-20.4661175769582,21.1068878832106,0.712445699282781));
#59417=CARTESIAN_POINT('Ctrl Pts',(-20.3968598474688,21.1998050042915,0.718299147582536));
#59418=CARTESIAN_POINT('Ctrl Pts',(-20.3275233569016,21.292827792316,0.724159252524087));
#59419=CARTESIAN_POINT('Ctrl Pts',(-20.2623550473619,21.3888560804346,0.730019357465638));
#59420=CARTESIAN_POINT('Ctrl Pts',(-20.2016070128739,21.4874723230232,0.735879462407188));
#59421=CARTESIAN_POINT('Ctrl Pts',(-20.1408180683868,21.586154977479,0.741743513762649));
#59422=CARTESIAN_POINT('Ctrl Pts',(-20.0844555268447,21.6874286963877,0.74760756511811));
#59423=CARTESIAN_POINT('Ctrl Pts',(-20.032724952684,21.7908524262881,0.75347161647357));
#59424=CARTESIAN_POINT('Ctrl Pts',(-19.9809181379835,21.8944285821209,0.759344310270141));
#59425=CARTESIAN_POINT('Ctrl Pts',(-19.9337570829936,22.0001606969211,0.765217004066713));
#59426=CARTESIAN_POINT('Ctrl Pts',(-19.8913988239385,22.1075888337928,0.771089697863284));
#59427=CARTESIAN_POINT('Ctrl Pts',(-19.8798018411765,22.1370008606147,0.772697543186596));
#59428=CARTESIAN_POINT('Ctrl Pts',(-19.868564571837,22.1665399381564,0.774305388509909));
#59429=CARTESIAN_POINT('Ctrl Pts',(-19.8576895767773,22.1961964678715,0.775913233833221));
#59430=CARTESIAN_POINT('Ctrl Pts',(-19.8179710792338,22.3045103380075,0.781785530801923));
#59431=CARTESIAN_POINT('Ctrl Pts',(-19.7829558356901,22.4147547376324,0.787657827770625));
#59432=CARTESIAN_POINT('Ctrl Pts',(-19.7528341943719,22.5264835287602,0.793530124739327));
#59433=CARTESIAN_POINT('Ctrl Pts',(-19.7227515883086,22.6380675282483,0.799394811677539));
#59434=CARTESIAN_POINT('Ctrl Pts',(-19.6975500796778,22.7511316983346,0.80525949861575));
#59435=CARTESIAN_POINT('Ctrl Pts',(-19.6773715272965,22.8652111272698,0.811124185553962));
#59436=CARTESIAN_POINT('Ctrl Pts',(-19.6572137272932,22.9791732326535,0.816982841028771));
#59437=CARTESIAN_POINT('Ctrl Pts',(-19.6420686800746,23.0941481154408,0.82284149650358));
#59438=CARTESIAN_POINT('Ctrl Pts',(-19.6320279224084,23.2096575945813,0.828700151978389));
#59439=CARTESIAN_POINT('Ctrl Pts',(-19.6215949639039,23.3296789757166,0.834787651696293));
#59440=CARTESIAN_POINT('Ctrl Pts',(-19.6166732984749,23.4502771292055,0.840875151414198));
#59441=CARTESIAN_POINT('Ctrl Pts',(-19.6173067598043,23.5709057487116,0.846962651132102));
#59442=CARTESIAN_POINT('Ctrl Pts',(-19.6179157016645,23.6868651807281,0.8528145212155));
#59443=CARTESIAN_POINT('Ctrl Pts',(-19.6236577182559,23.8028523121815,0.858666391298898));
#59444=CARTESIAN_POINT('Ctrl Pts',(-19.6345186823776,23.9183794409474,0.864518261382296));
#59445=CARTESIAN_POINT('Ctrl Pts',(-19.6453779928187,24.0338889796573,0.870369240465256));
#59446=CARTESIAN_POINT('Ctrl Pts',(-19.6613546623991,24.1489382434858,0.876220219548216));
#59447=CARTESIAN_POINT('Ctrl Pts',(-19.6823825994137,24.2630436560501,0.882071198631177));
#59448=CARTESIAN_POINT('Ctrl Pts',(-19.7034124270423,24.3771593277895,0.887922703773483));
#59449=CARTESIAN_POINT('Ctrl Pts',(-19.7294943500053,24.4903305730067,0.893774208915788));
#59450=CARTESIAN_POINT('Ctrl Pts',(-19.7605110984266,24.6020837296412,0.899625714058094));
#59451=CARTESIAN_POINT('Ctrl Pts',(-19.7915381468347,24.7138739970659,0.905479162357853));
#59452=CARTESIAN_POINT('Ctrl Pts',(-19.8275031687529,24.8242448414057,0.911332610657612));
#59453=CARTESIAN_POINT('Ctrl Pts',(-19.868239162872,24.932738174229,0.917186058957371));
#59454=CARTESIAN_POINT('Ctrl Pts',(-19.9090214826623,25.041354887531,0.923046163898914));
#59455=CARTESIAN_POINT('Ctrl Pts',(-19.9545854586558,25.1480894404129,0.928906268840457));
#59456=CARTESIAN_POINT('Ctrl Pts',(-20.0047160702204,25.2525040408314,0.934766373782001));
#59457=CARTESIAN_POINT('Ctrl Pts',(-20.0548804416144,25.3569889579484,0.940630425137458));
#59458=CARTESIAN_POINT('Ctrl Pts',(-20.1096173774465,25.4591504481802,0.946494476492915));
#59459=CARTESIAN_POINT('Ctrl Pts',(-20.168666928332,25.5585771586242,0.952358527848371));
#59460=CARTESIAN_POINT('Ctrl Pts',(-20.2278035064681,25.6581504041919,0.958231221644946));
#59461=CARTESIAN_POINT('Ctrl Pts',(-20.291265159128,25.7549804813868,0.964103915441522));
#59462=CARTESIAN_POINT('Ctrl Pts',(-20.3587498184206,25.8486866576085,0.969976609238097));
#59463=CARTESIAN_POINT('Ctrl Pts',(-20.3772259892545,25.8743418411452,0.971584454561435));
#59464=CARTESIAN_POINT('Ctrl Pts',(-20.396003490345,25.8997630680443,0.973192299884774));
#59465=CARTESIAN_POINT('Ctrl Pts',(-20.4150756305256,25.9249429953923,0.974800145208113));
#59466=CARTESIAN_POINT('Ctrl Pts',(-20.4847323750791,26.0169070723418,0.980672442176815));
#59467=CARTESIAN_POINT('Ctrl Pts',(-20.5585556146544,26.1059577558187,0.986544739145517));
#59468=CARTESIAN_POINT('Ctrl Pts',(-20.636272897164,26.1916937461722,0.992417036114219));
#59469=CARTESIAN_POINT('Ctrl Pts',(-20.7138894642477,26.2773186294914,0.998281723052427));
#59470=CARTESIAN_POINT('Ctrl Pts',(-20.7953897637771,26.3596370586016,1.00414640999064));
#59471=CARTESIAN_POINT('Ctrl Pts',(-20.8804593384015,26.4382783807904,1.01001109692884));
#59472=CARTESIAN_POINT('Ctrl Pts',(-20.9654414242936,26.5168388253022,1.01586975240365));
#59473=CARTESIAN_POINT('Ctrl Pts',(-21.0539851821937,26.5917294059123,1.02172840787846));
#59474=CARTESIAN_POINT('Ctrl Pts',(-21.1457377898646,26.6626146340731,1.02758706335327));
#59475=CARTESIAN_POINT('Ctrl Pts',(-21.2410743352061,26.7362687016809,1.03367456307118));
#59476=CARTESIAN_POINT('Ctrl Pts',(-21.3398752163534,26.8055977958626,1.03976206278909));
#59477=CARTESIAN_POINT('Ctrl Pts',(-21.4417045105835,26.870269736871,1.04584956250699));
#59478=CARTESIAN_POINT('Ctrl Pts',(-21.5395922852253,26.9324384127412,1.05170143259039));
#59479=CARTESIAN_POINT('Ctrl Pts',(-21.6402780083667,26.9903035194359,1.05755330267378));
#59480=CARTESIAN_POINT('Ctrl Pts',(-21.7433437316768,27.0436133187329,1.06340517275718));
#59481=CARTESIAN_POINT('Ctrl Pts',(-21.8463937622933,27.0969150011283,1.06925615184014));
#59482=CARTESIAN_POINT('Ctrl Pts',(-21.9518227054845,27.1456625653336,1.0751071309231));
#59483=CARTESIAN_POINT('Ctrl Pts',(-22.0591879949576,27.1896502218741,1.08095811000606));
#59484=CARTESIAN_POINT('Ctrl Pts',(-22.1665629376033,27.2336418333281,1.08680961514834));
#59485=CARTESIAN_POINT('Ctrl Pts',(-22.2758741900719,27.2728725296398,1.09266112029062));
#59486=CARTESIAN_POINT('Ctrl Pts',(-22.386659863185,27.3071849374997,1.0985126254329));
#59487=CARTESIAN_POINT('Ctrl Pts',(-22.497482325809,27.3415087397636,1.10436607373268));
#59488=CARTESIAN_POINT('Ctrl Pts',(-22.6097797879941,27.3709108837117,1.11021952203246));
#59489=CARTESIAN_POINT('Ctrl Pts',(-22.7230765809695,27.3952842541307,1.11607297033224));
#59490=CARTESIAN_POINT('Ctrl Pts',(-22.8365022170003,27.4196853423643,1.12193307527378));
#59491=CARTESIAN_POINT('Ctrl Pts',(-22.950929047777,27.4390461555089,1.12779318021532));
#59492=CARTESIAN_POINT('Ctrl Pts',(-23.0658725237412,27.4533109488711,1.13365328515686));
#59493=CARTESIAN_POINT('Ctrl Pts',(-23.1808934069419,27.4675853486788,1.13951733651228));
#59494=CARTESIAN_POINT('Ctrl Pts',(-23.2964312170446,27.4767568625767,1.14538138786771));
#59495=CARTESIAN_POINT('Ctrl Pts',(-23.4119993622882,27.4808218366613,1.15124543922313));
#59496=CARTESIAN_POINT('Ctrl Pts',(-23.527737831909,27.4848928017062,1.15711813301971));
#59497=CARTESIAN_POINT('Ctrl Pts',(-23.6435063140853,27.4838422101904,1.16299082681629));
#59498=CARTESIAN_POINT('Ctrl Pts',(-23.7588212115915,27.4777183947878,1.16886352061288));
#59499=CARTESIAN_POINT('Ctrl Pts',(-23.790392501547,27.4760417965695,1.17047136593626));
#59500=CARTESIAN_POINT('Ctrl Pts',(-23.8219298416358,27.4739852206697,1.17207921125964));
#59501=CARTESIAN_POINT('Ctrl Pts',(-23.8534234372826,27.4715503273232,1.17368705658302));
#59502=CARTESIAN_POINT('Ctrl Pts',(-23.9684467816063,27.4626574216374,1.17955935355172));
#59503=CARTESIAN_POINT('Ctrl Pts',(-24.0832712063095,27.4486843611038,1.18543165052042));
#59504=CARTESIAN_POINT('Ctrl Pts',(-24.1974118193595,27.4296434447614,1.19130394748912));
#59505=CARTESIAN_POINT('Ctrl Pts',(-24.3114045152403,27.4106272039344,1.19716863442735));
#59506=CARTESIAN_POINT('Ctrl Pts',(-24.4247147577485,27.386556235168,1.20303332136557));
#59507=CARTESIAN_POINT('Ctrl Pts',(-24.5368607330095,27.3574947432034,1.20889800830379));
#59508=CARTESIAN_POINT('Ctrl Pts',(-24.648891373155,27.3284631391641,1.21475666377861));
#59509=CARTESIAN_POINT('Ctrl Pts',(-24.7597597299366,27.2944513236904,1.22061531925343));
#59510=CARTESIAN_POINT('Ctrl Pts',(-24.8689928358335,27.2555747862678,1.22647397472825));
#59511=CARTESIAN_POINT('Ctrl Pts',(-24.982492683058,27.2151796970515,1.23256147444615));
#59512=CARTESIAN_POINT('Ctrl Pts',(-25.0942264779404,27.1695321725109,1.23864897416405));
#59513=CARTESIAN_POINT('Ctrl Pts',(-25.203679117374,27.1188194045112,1.24473647388195));
#59514=CARTESIAN_POINT('Ctrl Pts',(-25.3088951594163,27.0700695821448,1.25058834396536));
#59515=CARTESIAN_POINT('Ctrl Pts',(-25.4120029462824,27.0166395371803,1.25644021404876));
#59516=CARTESIAN_POINT('Ctrl Pts',(-25.5125647675914,26.9587448213801,1.26229208413216));
#59517=CARTESIAN_POINT('Ctrl Pts',(-25.6131112774487,26.9008589205767,1.26814306321514));
#59518=CARTESIAN_POINT('Ctrl Pts',(-25.7111122343585,26.8385099067658,1.27399404229811));
#59519=CARTESIAN_POINT('Ctrl Pts',(-25.8061552783399,26.7719588804598,1.27984502138109));
#59520=CARTESIAN_POINT('Ctrl Pts',(-25.9012068676054,26.7054018705761,1.28569652652338));
#59521=CARTESIAN_POINT('Ctrl Pts',(-25.993299676627,26.6346423342866,1.29154803166567));
#59522=CARTESIAN_POINT('Ctrl Pts',(-26.0820516339175,26.5599837997614,1.29739953680796));
#59523=CARTESIAN_POINT('Ctrl Pts',(-26.170833063801,26.485300472762,1.30325298510774));
#59524=CARTESIAN_POINT('Ctrl Pts',(-26.2562711197593,26.4067158389205,1.30910643340751));
#59525=CARTESIAN_POINT('Ctrl Pts',(-26.3380185648302,26.3245721860407,1.31495988170728));
#59526=CARTESIAN_POINT('Ctrl Pts',(-26.4198589744973,26.2423351179903,1.32081998664883));
#59527=CARTESIAN_POINT('Ctrl Pts',(-26.4980001043688,26.1565312456439,1.32668009159037));
#59528=CARTESIAN_POINT('Ctrl Pts',(-26.5721331359211,26.0675380963049,1.33254019653192));
#59529=CARTESIAN_POINT('Ctrl Pts',(-26.64631609143,25.97848501565,1.33840424788735));
#59530=CARTESIAN_POINT('Ctrl Pts',(-26.7164853243102,25.8862387095584,1.34426829924277));
#59531=CARTESIAN_POINT('Ctrl Pts',(-26.7823747369962,25.7912065807531,1.3501323505982));
#59532=CARTESIAN_POINT('Ctrl Pts',(-26.8483612575241,25.6960343935597,1.35600504439478));
#59533=CARTESIAN_POINT('Ctrl Pts',(-26.9100551496453,25.5980685378605,1.36187773819136));
#59534=CARTESIAN_POINT('Ctrl Pts',(-26.9672356716477,25.4977419979746,1.36775043198794));
#59535=CARTESIAN_POINT('Ctrl Pts',(-26.9828907420586,25.470274269612,1.36935827731127));
#59536=CARTESIAN_POINT('Ctrl Pts',(-26.9982077795287,25.4426297097966,1.3709661226346));
#59537=CARTESIAN_POINT('Ctrl Pts',(-27.0131828864579,25.4148174562963,1.37257396795793));
#59538=CARTESIAN_POINT('Ctrl Pts',(-27.0708508582076,25.3077146318063,1.37876565521078));
#59539=CARTESIAN_POINT('Ctrl Pts',(-27.1236204990138,25.1977965269381,1.38495734246363));
#59540=CARTESIAN_POINT('Ctrl Pts',(-27.1712229605583,25.0855251958459,1.39114902971648));
#59541=CARTESIAN_POINT('Ctrl Pts',(-27.2187367175758,24.9734630761055,1.39732917910613));
#59542=CARTESIAN_POINT('Ctrl Pts',(-27.2611023414214,24.8590567836819,1.40350932849577));
#59543=CARTESIAN_POINT('Ctrl Pts',(-27.2980967767422,24.7427928936361,1.40968947788542));
#59544=CARTESIAN_POINT('Ctrl Pts',(-27.335001395954,24.6268112722648,1.41585462293816));
#59545=CARTESIAN_POINT('Ctrl Pts',(-27.366560718547,24.508981373887,1.4220197679909));
#59546=CARTESIAN_POINT('Ctrl Pts',(-27.3926000459075,24.3898087120767,1.42818491304364));
#59547=CARTESIAN_POINT('Ctrl Pts',(-27.4186007329442,24.2708128931694,1.43434090950364));
#59548=CARTESIAN_POINT('Ctrl Pts',(-27.4390976638491,24.1504786166865,1.44049690596364));
#59549=CARTESIAN_POINT('Ctrl Pts',(-27.453965740447,24.0293268305339,1.44665290242364));
#59550=CARTESIAN_POINT('Ctrl Pts',(-27.468806040479,23.9084013803542,1.4527973982406));
#59551=CARTESIAN_POINT('Ctrl Pts',(-27.4780384049081,23.7866618085343,1.45894189405755));
#59552=CARTESIAN_POINT('Ctrl Pts',(-27.4815887897958,23.6646388321663,1.4650863898745));
#59553=CARTESIAN_POINT('Ctrl Pts',(-27.482696286455,23.6265753424482,1.46700308589613));
#59554=CARTESIAN_POINT('Ctrl Pts',(-27.4832512740033,23.5884843489477,1.46891978191775));
#59555=CARTESIAN_POINT('Ctrl Pts',(-27.4832525295589,23.5503821330864,1.47083647793938));
#59556=CARTESIAN_POINT('',(-27.4832508767861,23.5466445538181,2.72083647796517));
#59557=CARTESIAN_POINT('Ctrl Pts',(-27.4832525295589,23.5503821325739,1.47083647796516));
#59558=CARTESIAN_POINT('Ctrl Pts',(-27.4832565348913,23.4288322440574,1.47695093043155));
#59559=CARTESIAN_POINT('Ctrl Pts',(-27.4776214550004,23.3073853627606,1.48306538289793));
#59560=CARTESIAN_POINT('Ctrl Pts',(-27.4664017061686,23.1865704682608,1.48917983536432));
#59561=CARTESIAN_POINT('Ctrl Pts',(-27.4551673184688,23.0655979415951,1.49530226560852));
#59562=CARTESIAN_POINT('Ctrl Pts',(-27.4383337613979,22.9452594005174,1.50142469585272));
#59563=CARTESIAN_POINT('Ctrl Pts',(-27.4160068384167,22.8260753157752,1.50754712609692));
#59564=CARTESIAN_POINT('Ctrl Pts',(-27.3936277081329,22.7066125415072,1.51368387249068));
#59565=CARTESIAN_POINT('Ctrl Pts',(-27.36572960262,22.5883099702222,1.51982061888443));
#59566=CARTESIAN_POINT('Ctrl Pts',(-27.3324690086286,22.4716759133652,1.52595736527819));
#59567=CARTESIAN_POINT('Ctrl Pts',(-27.2991660722478,22.3548933755562,1.53210192405514));
#59568=CARTESIAN_POINT('Ctrl Pts',(-27.2604871411608,22.2397839267865,1.53824648283209));
#59569=CARTESIAN_POINT('Ctrl Pts',(-27.216637287345,22.1268369832575,1.54439104160904));
#59570=CARTESIAN_POINT('Ctrl Pts',(-27.1726892208608,22.013637066919,1.55054936265568));
#59571=CARTESIAN_POINT('Ctrl Pts',(-27.1235472255114,21.9026096631,1.55670768370233));
#59572=CARTESIAN_POINT('Ctrl Pts',(-27.0694633883307,21.7942217954791,1.56286600474897));
#59573=CARTESIAN_POINT('Ctrl Pts',(-27.0443026454344,21.7437978719478,1.56573096294358));
#59574=CARTESIAN_POINT('Ctrl Pts',(-27.0180729803856,21.6939448245498,1.5685959211382));
#59575=CARTESIAN_POINT('Ctrl Pts',(-26.9908029476806,21.6447075085956,1.57146087933281));
#59576=CARTESIAN_POINT('Ctrl Pts',(-26.9349076362968,21.5437859168715,1.57733317630148));
#59577=CARTESIAN_POINT('Ctrl Pts',(-26.874474423979,21.4451567032586,1.58320547327015));
#59578=CARTESIAN_POINT('Ctrl Pts',(-26.8097160317601,21.3492557820968,1.58907777023883));
#59579=CARTESIAN_POINT('Ctrl Pts',(-26.7450415612745,21.2534791409125,1.594942457177));
#59580=CARTESIAN_POINT('Ctrl Pts',(-26.6760532866023,21.1604241004678,1.60080714411518));
#59581=CARTESIAN_POINT('Ctrl Pts',(-26.6030098594493,21.0705022019559,1.60667183105336));
#59582=CARTESIAN_POINT('Ctrl Pts',(-26.5300415528889,20.9806727824878,1.61253048652813));
#59583=CARTESIAN_POINT('Ctrl Pts',(-26.4530266481982,20.8939704146855,1.6183891420029));
#59584=CARTESIAN_POINT('Ctrl Pts',(-26.3722667655501,20.8107772783081,1.62424779747767));
#59585=CARTESIAN_POINT('Ctrl Pts',(-26.2883523307525,20.7243345447474,1.63033529719559));
#59586=CARTESIAN_POINT('Ctrl Pts',(-26.2003946439296,20.6416811555589,1.6364227969135));
#59587=CARTESIAN_POINT('Ctrl Pts',(-26.1087780537844,20.5632078127767,1.64251029663142));
#59588=CARTESIAN_POINT('Ctrl Pts',(-26.0207076787775,20.4877719477666,1.64836216671479));
#59589=CARTESIAN_POINT('Ctrl Pts',(-25.929256728141,20.4161988449634,1.65421403679816));
#59590=CARTESIAN_POINT('Ctrl Pts',(-25.8348031783186,20.3487970278634,1.66006590688154));
#59591=CARTESIAN_POINT('Ctrl Pts',(-25.740364009908,20.2814054733031,1.66591688596448));
#59592=CARTESIAN_POINT('Ctrl Pts',(-25.6429234877185,20.2181841816864,1.67176786504742));
#59593=CARTESIAN_POINT('Ctrl Pts',(-25.5428904800334,20.1593996881107,1.67761884413036));
#59594=CARTESIAN_POINT('Ctrl Pts',(-25.4428484784184,20.1006099092434,1.68347034927262));
#59595=CARTESIAN_POINT('Ctrl Pts',(-25.3402138843688,20.0462579308662,1.68932185441488));
#59596=CARTESIAN_POINT('Ctrl Pts',(-25.2354215668566,19.9965651055227,1.69517335955713));
#59597=CARTESIAN_POINT('Ctrl Pts',(-25.1305944500972,19.9468557782736,1.70102680785686));
#59598=CARTESIAN_POINT('Ctrl Pts',(-25.0236085584117,19.9018088576026,1.70688025615659));
#59599=CARTESIAN_POINT('Ctrl Pts',(-24.9149195358079,19.8615979032581,1.71273370445632));
#59600=CARTESIAN_POINT('Ctrl Pts',(-24.8061069101838,19.8213412203267,1.71859380939783));
#59601=CARTESIAN_POINT('Ctrl Pts',(-24.6955876757186,19.7859316241654,1.72445391433934));
#59602=CARTESIAN_POINT('Ctrl Pts',(-24.5838335601979,19.7554930850998,1.73031401928085));
#59603=CARTESIAN_POINT('Ctrl Pts',(-24.4720041852746,19.7250340475833,1.73617807063628));
#59604=CARTESIAN_POINT('Ctrl Pts',(-24.3589386756682,19.699552823751,1.74204212199172));
#59605=CARTESIAN_POINT('Ctrl Pts',(-24.2451181758774,19.6791221106758,1.74790617334715));
#59606=CARTESIAN_POINT('Ctrl Pts',(-24.1311299273907,19.658661286808,1.7537788671437));
#59607=CARTESIAN_POINT('Ctrl Pts',(-24.0163848761487,19.6432658841415,1.75965156094026));
#59608=CARTESIAN_POINT('Ctrl Pts',(-23.9013685828456,19.6329567146,1.76552425473681));
#59609=CARTESIAN_POINT('Ctrl Pts',(-23.8698790457211,19.6301342364304,1.76713210006043));
#59610=CARTESIAN_POINT('Ctrl Pts',(-23.838369170144,19.6276927070489,1.76873994538405));
#59611=CARTESIAN_POINT('Ctrl Pts',(-23.8068488871828,19.6256318735477,1.77034779070766));
#59612=CARTESIAN_POINT('Ctrl Pts',(-23.691728073404,19.6181051381433,1.77622008767637));
#59613=CARTESIAN_POINT('Ctrl Pts',(-23.576082947962,19.6156353424828,1.78209238464508));
#59614=CARTESIAN_POINT('Ctrl Pts',(-23.4603952376413,19.6182791509723,1.78796468161378));
#59615=CARTESIAN_POINT('Ctrl Pts',(-23.3448574494052,19.620919533296,1.79382936855199));
#59616=CARTESIAN_POINT('Ctrl Pts',(-23.2292775954971,19.6286603320366,1.7996940554902));
#59617=CARTESIAN_POINT('Ctrl Pts',(-23.1141417246397,19.6415063946356,1.80555874242841));
#59618=CARTESIAN_POINT('Ctrl Pts',(-22.9991242638178,19.6543392458635,1.81141739790324));
#59619=CARTESIAN_POINT('Ctrl Pts',(-22.884550286192,19.6722668719838,1.81727605337807));
#59620=CARTESIAN_POINT('Ctrl Pts',(-22.7709043644959,19.695242099246,1.8231347088529));
#59621=CARTESIAN_POINT('Ctrl Pts',(-22.6528193330005,19.7191147591213,1.82922220857081));
#59622=CARTESIAN_POINT('Ctrl Pts',(-22.5357367913787,19.748437376039,1.83530970828871));
#59623=CARTESIAN_POINT('Ctrl Pts',(-22.4201932005747,19.7830977819992,1.84139720800661));
#59624=CARTESIAN_POINT('Ctrl Pts',(-22.3091219704004,19.816416583168,1.84724907809001));
#59625=CARTESIAN_POINT('Ctrl Pts',(-22.1994732024405,19.8546675060611,1.8531009481734));
#59626=CARTESIAN_POINT('Ctrl Pts',(-22.0917107749805,19.8976993227837,1.85895281825679));
#59627=CARTESIAN_POINT('Ctrl Pts',(-21.9839647553298,19.9407245875209,1.86480379733975));
#59628=CARTESIAN_POINT('Ctrl Pts',(-21.8781048889094,19.988529145461,1.87065477642272));
#59629=CARTESIAN_POINT('Ctrl Pts',(-21.774576426809,20.0409130823762,1.87650575550569));
#59630=CARTESIAN_POINT('Ctrl Pts',(-21.6710386565036,20.0933017291114,1.88235726064798));
#59631=CARTESIAN_POINT('Ctrl Pts',(-21.5698330760904,20.1502703866578,1.88820876579028));
#59632=CARTESIAN_POINT('Ctrl Pts',(-21.4713809782929,20.2115728428862,1.89406027093257));
#59633=CARTESIAN_POINT('Ctrl Pts',(-21.372896186697,20.2728956563258,1.89991371923234));
#59634=CARTESIAN_POINT('Ctrl Pts',(-21.2771670466177,20.3385549117402,1.9057671675321));
#59635=CARTESIAN_POINT('Ctrl Pts',(-21.1845858716859,20.4082610845822,1.91162061583187));
#59636=CARTESIAN_POINT('Ctrl Pts',(-21.0918994118545,20.4780465284792,1.9174807207734));
#59637=CARTESIAN_POINT('Ctrl Pts',(-21.0023683930215,20.5518878269099,1.92334082571494));
#59638=CARTESIAN_POINT('Ctrl Pts',(-20.9163521023681,20.6294551185901,1.92920093065647));
#59639=CARTESIAN_POINT('Ctrl Pts',(-20.8302778851264,20.7070746469865,1.93506498201192));
#59640=CARTESIAN_POINT('Ctrl Pts',(-20.7477234028567,20.7884248755529,1.94092903336736));
#59641=CARTESIAN_POINT('Ctrl Pts',(-20.6690098958248,20.8731403051994,1.94679308472281));
#59642=CARTESIAN_POINT('Ctrl Pts',(-20.5901803807961,20.9579805884783,1.95266577851937));
#59643=CARTESIAN_POINT('Ctrl Pts',(-20.5152034056408,21.0461956575109,1.95853847231594));
#59644=CARTESIAN_POINT('Ctrl Pts',(-20.4443589459188,21.1373882516653,1.96441116611251));
#59645=CARTESIAN_POINT('Ctrl Pts',(-20.4249629179298,21.1623552584793,1.96601901143586));
#59646=CARTESIAN_POINT('Ctrl Pts',(-20.4058763947519,21.1875452953443,1.96762685675921));
#59647=CARTESIAN_POINT('Ctrl Pts',(-20.3871045317731,21.2129498703781,1.96923470208257));
#59648=CARTESIAN_POINT('Ctrl Pts',(-20.3185444828267,21.3057344229689,1.97510699905128));
#59649=CARTESIAN_POINT('Ctrl Pts',(-20.2539555094522,21.4016935780694,1.98097929602));
#59650=CARTESIAN_POINT('Ctrl Pts',(-20.1936456781143,21.5004526803671,1.98685159298872));
#59651=CARTESIAN_POINT('Ctrl Pts',(-20.1334140035282,21.5990837987113,1.99271627992692));
#59652=CARTESIAN_POINT('Ctrl Pts',(-20.0774506565707,21.7005072989065,1.99858096686513));
#59653=CARTESIAN_POINT('Ctrl Pts',(-20.0260224454153,21.8043168802549,2.00444565380333));
#59654=CARTESIAN_POINT('Ctrl Pts',(-19.9746471249556,21.9080196999476,2.01030430927816));
#59655=CARTESIAN_POINT('Ctrl Pts',(-19.9277978455624,22.0141033515988,2.01616296475299));
#59656=CARTESIAN_POINT('Ctrl Pts',(-19.8856968512728,22.1221346566254,2.02202162022782));
#59657=CARTESIAN_POINT('Ctrl Pts',(-19.8419513550642,22.2343857595787,2.02810911994572));
#59658=CARTESIAN_POINT('Ctrl Pts',(-19.8033328874315,22.3487393838029,2.03419661966362));
#59659=CARTESIAN_POINT('Ctrl Pts',(-19.7700370594367,22.4646835641454,2.04028411938152));
#59660=CARTESIAN_POINT('Ctrl Pts',(-19.7380300173382,22.5761398781879,2.04613598946493));
#59661=CARTESIAN_POINT('Ctrl Pts',(-19.7109413531281,22.6890654717823,2.05198785954834));
#59662=CARTESIAN_POINT('Ctrl Pts',(-19.6888945821195,22.802988331256,2.05783972963174));
#59663=CARTESIAN_POINT('Ctrl Pts',(-19.6668511679323,22.9168938449386,2.06369070871472));
#59664=CARTESIAN_POINT('Ctrl Pts',(-19.6498481990855,23.0317959168469,2.0695416877977));
#59665=CARTESIAN_POINT('Ctrl Pts',(-19.6379581614747,23.1472118876537,2.07539266688068));
#59666=CARTESIAN_POINT('Ctrl Pts',(-19.6260670548351,23.2626382354668,2.08124417202299));
#59667=CARTESIAN_POINT('Ctrl Pts',(-19.6192898356407,23.3785781627976,2.08709567716529));
#59668=CARTESIAN_POINT('Ctrl Pts',(-19.6176470880733,23.4945441409154,2.0929471823076));
#59669=CARTESIAN_POINT('Ctrl Pts',(-19.6160037949852,23.6105486288105,2.0988006306074));
#59670=CARTESIAN_POINT('Ctrl Pts',(-19.6194983697534,23.7265787715718,2.1046540789072));
#59671=CARTESIAN_POINT('Ctrl Pts',(-19.6280992926678,23.8421480088679,2.110507527207));
#59672=CARTESIAN_POINT('Ctrl Pts',(-19.6367099966991,23.9578486734819,2.11636763214855));
#59673=CARTESIAN_POINT('Ctrl Pts',(-19.650438608828,24.0730869739565,2.12222773709011));
#59674=CARTESIAN_POINT('Ctrl Pts',(-19.6692018211744,24.18738233195,2.12808784203166));
#59675=CARTESIAN_POINT('Ctrl Pts',(-19.68797766937,24.3017546607135,2.1339518933871));
#59676=CARTESIAN_POINT('Ctrl Pts',(-19.7117947841775,24.4151823789874,2.13981594474255));
#59677=CARTESIAN_POINT('Ctrl Pts',(-19.7405193090625,24.5271976541939,2.14567999609799));
#59678=CARTESIAN_POINT('Ctrl Pts',(-19.7692861681632,24.6393780175559,2.15155268989457));
#59679=CARTESIAN_POINT('Ctrl Pts',(-19.8029747522637,24.7501413892508,2.15742538369115));
#59680=CARTESIAN_POINT('Ctrl Pts',(-19.8414021779883,24.8590374849297,2.16329807748773));
#59681=CARTESIAN_POINT('Ctrl Pts',(-19.8519229643388,24.8888514143157,2.16490592281098));
#59682=CARTESIAN_POINT('Ctrl Pts',(-19.8627986900844,24.9185255093086,2.16651376813422));
#59683=CARTESIAN_POINT('Ctrl Pts',(-19.8740249975681,24.9480508423717,2.16812161345746));
#59684=CARTESIAN_POINT('Ctrl Pts',(-19.9150265855024,25.0558855459591,2.17399391042616));
#59685=CARTESIAN_POINT('Ctrl Pts',(-19.9608455544848,25.1620953242776,2.17986620739486));
#59686=CARTESIAN_POINT('Ctrl Pts',(-20.0113332236989,25.2662184787625,2.18573850436356));
#59687=CARTESIAN_POINT('Ctrl Pts',(-20.0617554649033,25.3702066979084,2.19160319130175));
#59688=CARTESIAN_POINT('Ctrl Pts',(-20.1168341958406,25.4721133021733,2.19746787823994));
#59689=CARTESIAN_POINT('Ctrl Pts',(-20.1763718100455,25.5714941986126,2.20333256517813));
#59690=CARTESIAN_POINT('Ctrl Pts',(-20.2358481935414,25.6707728880215,2.20919122065295));
#59691=CARTESIAN_POINT('Ctrl Pts',(-20.2997741279791,25.7675306837463,2.21504987612777));
#59692=CARTESIAN_POINT('Ctrl Pts',(-20.3679053052723,25.8613464567619,2.22090853160259));
#59693=CARTESIAN_POINT('Ctrl Pts',(-20.4386977463598,25.9588267565034,2.22699603132049));
#59694=CARTESIAN_POINT('Ctrl Pts',(-20.5140304501644,26.0531301029606,2.2330835310384));
#59695=CARTESIAN_POINT('Ctrl Pts',(-20.5935784278852,26.1438151863963,2.23917103075631));
#59696=CARTESIAN_POINT('Ctrl Pts',(-20.6700473318014,26.2309901106441,2.2450229008397));
#59697=CARTESIAN_POINT('Ctrl Pts',(-20.7504109570101,26.3148213289378,2.25087477092309));
#59698=CARTESIAN_POINT('Ctrl Pts',(-20.8343389557518,26.3949497823717,2.25672664100648));
#59699=CARTESIAN_POINT('Ctrl Pts',(-20.9182541756929,26.4750660355201,2.26257762008945));
#59700=CARTESIAN_POINT('Ctrl Pts',(-21.0057323911758,26.551480359402,2.26842859917242));
#59701=CARTESIAN_POINT('Ctrl Pts',(-21.0964067145099,26.6238708725893,2.27427957825539));
#59702=CARTESIAN_POINT('Ctrl Pts',(-21.1870891903378,26.6962678943801,2.28013108339766));
#59703=CARTESIAN_POINT('Ctrl Pts',(-21.280968022188,26.7646401283626,2.28598258853994));
#59704=CARTESIAN_POINT('Ctrl Pts',(-21.3776441705826,26.8287067267727,2.29183409368221));
#59705=CARTESIAN_POINT('Ctrl Pts',(-21.4743524230222,26.892794600306,2.297687541982));
#59706=CARTESIAN_POINT('Ctrl Pts',(-21.5738594947173,26.9525737669501,2.30354099028179));
#59707=CARTESIAN_POINT('Ctrl Pts',(-21.6757389965578,27.0078077382803,2.30939443858158));
#59708=CARTESIAN_POINT('Ctrl Pts',(-21.7777343575141,27.0631045226294,2.31525454352312));
#59709=CARTESIAN_POINT('Ctrl Pts',(-21.8821071700526,27.1138455976081,2.32111464846465));
#59710=CARTESIAN_POINT('Ctrl Pts',(-21.9884080841103,27.1598412785671,2.32697475340619));
#59711=CARTESIAN_POINT('Ctrl Pts',(-22.0947805851808,27.2058679347385,2.33283880476165));
#59712=CARTESIAN_POINT('Ctrl Pts',(-22.2030833879159,27.2471426867111,2.33870285611711));
#59713=CARTESIAN_POINT('Ctrl Pts',(-22.3128505417866,27.2835252668922,2.34456690747257));
#59714=CARTESIAN_POINT('Ctrl Pts',(-22.4227794705302,27.3199614677337,2.35043960126913));
#59715=CARTESIAN_POINT('Ctrl Pts',(-22.5341766614188,27.3514909946883,2.3563122950657));
#59716=CARTESIAN_POINT('Ctrl Pts',(-22.6465644264571,27.3780243128292,2.36218498886226));
#59717=CARTESIAN_POINT('Ctrl Pts',(-22.6773343165076,27.3852886914881,2.36379283418562));
#59718=CARTESIAN_POINT('Ctrl Pts',(-22.708178421327,27.392178867261,2.36540067950899));
#59719=CARTESIAN_POINT('Ctrl Pts',(-22.7390868745305,27.3986936806061,2.36700852483235));
#59720=CARTESIAN_POINT('Ctrl Pts',(-22.8519731163951,27.4224875854688,2.37288082180105));
#59721=CARTESIAN_POINT('Ctrl Pts',(-22.9660962800474,27.4413502058351,2.37875311876975));
#59722=CARTESIAN_POINT('Ctrl Pts',(-23.080987562454,27.4551570617236,2.38462541573845));
#59723=CARTESIAN_POINT('Ctrl Pts',(-23.1957299548836,27.4689460250234,2.39049010267667));
#59724=CARTESIAN_POINT('Ctrl Pts',(-23.3112380798912,27.4776922042941,2.39635478961489));
#59725=CARTESIAN_POINT('Ctrl Pts',(-23.4270314999599,27.4813217981074,2.40221947655312));
#59726=CARTESIAN_POINT('Ctrl Pts',(-23.5427058337444,27.4849476591106,2.40807813202794));
#59727=CARTESIAN_POINT('Ctrl Pts',(-23.6586644682903,27.4834673883464,2.41393678750276));
#59728=CARTESIAN_POINT('Ctrl Pts',(-23.774421041805,27.4768588882157,2.41979544297758));
#59729=CARTESIAN_POINT('Ctrl Pts',(-23.8946991690384,27.4699922542491,2.42588294269548));
#59730=CARTESIAN_POINT('Ctrl Pts',(-24.014758676644,27.4575885431502,2.43197044241338));
#59731=CARTESIAN_POINT('Ctrl Pts',(-24.1340526131114,27.4396826268286,2.43805794213129));
#59732=CARTESIAN_POINT('Ctrl Pts',(-24.2487290238372,27.422469797113,2.44390981221469));
#59733=CARTESIAN_POINT('Ctrl Pts',(-24.3626975806099,27.4001728582094,2.44976168229809));
#59734=CARTESIAN_POINT('Ctrl Pts',(-24.4754776341793,27.3728756506704,2.45561355238148));
#59735=CARTESIAN_POINT('Ctrl Pts',(-24.5882405159602,27.3455825993795,2.46146453146446));
#59736=CARTESIAN_POINT('Ctrl Pts',(-24.6998148526737,27.3132908904538,2.46731551054743));
#59737=CARTESIAN_POINT('Ctrl Pts',(-24.8097315217236,27.276135202106,2.4731664896304));
#59738=CARTESIAN_POINT('Ctrl Pts',(-24.9196580733395,27.2389761731043,2.47901799477268));
#59739=CARTESIAN_POINT('Ctrl Pts',(-25.0279262693765,27.1969524277186,2.48486949991497));
#59740=CARTESIAN_POINT('Ctrl Pts',(-25.1340841301445,27.1502478744343,2.49072100505725));
#59741=CARTESIAN_POINT('Ctrl Pts',(-25.2402772436273,27.1035278115845,2.49657445335703));
#59742=CARTESIAN_POINT('Ctrl Pts',(-25.3443582501698,27.0521240164031,2.5024279016568));
#59743=CARTESIAN_POINT('Ctrl Pts',(-25.4458977067021,26.9962673851835,2.50828134995658));
#59744=CARTESIAN_POINT('Ctrl Pts',(-25.5475526356453,26.9403472328453,2.51414145489812));
#59745=CARTESIAN_POINT('Ctrl Pts',(-25.6466598832259,26.8799643365566,2.52000155983966));
#59746=CARTESIAN_POINT('Ctrl Pts',(-25.7428169718074,26.8153942094704,2.5258616647812));
#59747=CARTESIAN_POINT('Ctrl Pts',(-25.8390388161701,26.7507805984446,2.53172571613667));
#59748=CARTESIAN_POINT('Ctrl Pts',(-25.9323062136828,26.6819743865744,2.53758976749214));
#59749=CARTESIAN_POINT('Ctrl Pts',(-26.0222492888522,26.6092917652773,2.54345381884761));
#59750=CARTESIAN_POINT('Ctrl Pts',(-26.1123249221597,26.5365020243055,2.54932651264417));
#59751=CARTESIAN_POINT('Ctrl Pts',(-26.1990661463341,26.4598247445117,2.55519920644074));
#59752=CARTESIAN_POINT('Ctrl Pts',(-26.2821394235273,26.3796134153976,2.5610719002373));
#59753=CARTESIAN_POINT('Ctrl Pts',(-26.3048834971763,26.3576528952579,2.56267974556062));
#59754=CARTESIAN_POINT('Ctrl Pts',(-26.3273528638878,26.3354276644646,2.56428759088393));
#59755=CARTESIAN_POINT('Ctrl Pts',(-26.3495412149203,26.312945396991,2.56589543620725));
#59756=CARTESIAN_POINT('Ctrl Pts',(-26.4294861757714,26.2319414508042,2.57168852697089));
#59757=CARTESIAN_POINT('Ctrl Pts',(-26.5060637743932,26.1473106300145,2.57748161773453));
#59758=CARTESIAN_POINT('Ctrl Pts',(-26.5789200013633,26.0593683835768,2.58327470849818));
#59759=CARTESIAN_POINT('Ctrl Pts',(-26.6516601170014,25.9715662911354,2.5890585667842));
#59760=CARTESIAN_POINT('Ctrl Pts',(-26.7206903918569,25.8804635973304,2.59484242507023));
#59761=CARTESIAN_POINT('Ctrl Pts',(-26.7856929894963,25.7864130903342,2.60062628335625));
#59762=CARTESIAN_POINT('Ctrl Pts',(-26.8506363999539,25.6924482196766,2.60640487523318));
#59763=CARTESIAN_POINT('Ctrl Pts',(-26.9115591784749,25.5955412156709,2.6121834671101));
#59764=CARTESIAN_POINT('Ctrl Pts',(-26.9681833632604,25.4960782768803,2.61796205898703));
#59765=CARTESIAN_POINT('Ctrl Pts',(-27.0247705829217,25.3966802690004,2.62373687851178));
#59766=CARTESIAN_POINT('Ctrl Pts',(-27.0770645754825,25.294730010542,2.62951169803653));
#59767=CARTESIAN_POINT('Ctrl Pts',(-27.1248308756546,25.190642321619,2.63528651756128));
#59768=CARTESIAN_POINT('Ctrl Pts',(-27.17257829933,25.0865957665269,2.64105905496745));
#59769=CARTESIAN_POINT('Ctrl Pts',(-27.2158014107761,24.9804138465547,2.64683159237361));
#59770=CARTESIAN_POINT('Ctrl Pts',(-27.2543122718042,24.8725348168723,2.65260412977978));
#59771=CARTESIAN_POINT('Ctrl Pts',(-27.2928316263285,24.764631994678,2.65837794030794));
#59772=CARTESIAN_POINT('Ctrl Pts',(-27.3266365003827,24.6550317122609,2.66415175083611));
#59773=CARTESIAN_POINT('Ctrl Pts',(-27.355587737806,24.5441906430099,2.66992556136427));
#59774=CARTESIAN_POINT('Ctrl Pts',(-27.3845409577316,24.4333419836629,2.67569976726732));
#59775=CARTESIAN_POINT('Ctrl Pts',(-27.4086397803666,24.3212527826688,2.68147397317038));
#59776=CARTESIAN_POINT('Ctrl Pts',(-27.4277957832568,24.2083918271792,2.68724817907344));
#59777=CARTESIAN_POINT('Ctrl Pts',(-27.4469700873666,24.0954230468399,2.69302790152453));
#59778=CARTESIAN_POINT('Ctrl Pts',(-27.4611920749221,23.9816814607547,2.69880762397564));
#59779=CARTESIAN_POINT('Ctrl Pts',(-27.4704250188582,23.8676429393665,2.70458734642673));
#59780=CARTESIAN_POINT('Ctrl Pts',(-27.4790775289498,23.760773509207,2.71000372360621));
#59781=CARTESIAN_POINT('Ctrl Pts',(-27.4833490335356,23.6536436393539,2.71542010078569));
#59782=CARTESIAN_POINT('Ctrl Pts',(-27.4832508767861,23.5466445538181,2.72083647796517));
#59783=CARTESIAN_POINT('',(-27.4847337162098,23.55176910164,3.97083647796515));
#59784=CARTESIAN_POINT('Ctrl Pts',(-27.4837197232878,23.5466441237168,2.72083647796517));
#59785=CARTESIAN_POINT('Ctrl Pts',(-27.486410087491,23.2572272739644,2.73548510117082));
#59786=CARTESIAN_POINT('Ctrl Pts',(-27.3249482139625,21.6609649344543,2.81642936150173));
#59787=CARTESIAN_POINT('Ctrl Pts',(-25.146211310607,19.1806225235481,2.96366925895684));
#59788=CARTESIAN_POINT('Ctrl Pts',(-20.7366928686042,19.8455753724331,3.16255617033201));
#59789=CARTESIAN_POINT('Ctrl Pts',(-18.9125972064597,23.9148124258598,3.36144308170675));
#59790=CARTESIAN_POINT('Ctrl Pts',(-21.3501135798777,27.6490498461272,3.56032999308169));
#59791=CARTESIAN_POINT('Ctrl Pts',(-25.8093711089935,27.6168400551356,3.7592169044566));
#59792=CARTESIAN_POINT('Ctrl Pts',(-27.4491102260847,25.0237028729037,3.8960523994177));
#59793=CARTESIAN_POINT('Ctrl Pts',(-27.4894584729477,23.6353302575449,3.96659225725393));
#59794=CARTESIAN_POINT('Ctrl Pts',(-27.4890477443728,23.5517707645087,3.97083647796515));
#59795=CARTESIAN_POINT('',(-27.4825761731824,23.5531249265093,5.22083643712987));
#59796=CARTESIAN_POINT('Ctrl Pts',(-27.4832522395187,23.5517685305957,3.97083647796515));
#59797=CARTESIAN_POINT('Ctrl Pts',(-27.4832963124207,23.4374289286688,3.9766526763897));
#59798=CARTESIAN_POINT('Ctrl Pts',(-27.4783500636744,23.3228856127001,3.98246887481425));
#59799=CARTESIAN_POINT('Ctrl Pts',(-27.4683864150193,23.2086154840257,3.9882850732388));
#59800=CARTESIAN_POINT('Ctrl Pts',(-27.4584351814101,23.0944877398273,3.99409402448183));
#59801=CARTESIAN_POINT('Ctrl Pts',(-27.4434790122282,22.9806329226432,3.99990297572487));
#59802=CARTESIAN_POINT('Ctrl Pts',(-27.4235428263286,22.8675290931842,4.0057119269679));
#59803=CARTESIAN_POINT('Ctrl Pts',(-27.4036259005948,22.7545345322945,4.01151526623657));
#59804=CARTESIAN_POINT('Ctrl Pts',(-27.3787385972726,22.6422899296219,4.01731860550524));
#59805=CARTESIAN_POINT('Ctrl Pts',(-27.3489576702902,22.5312685916811,4.02312194477391));
#59806=CARTESIAN_POINT('Ctrl Pts',(-27.3191958220377,22.4203183779916,4.02892156621529));
#59807=CARTESIAN_POINT('Ctrl Pts',(-27.2845466920075,22.3105902772112,4.03472118765667));
#59808=CARTESIAN_POINT('Ctrl Pts',(-27.2451380415968,22.2025470487672,4.04052080909804));
#59809=CARTESIAN_POINT('Ctrl Pts',(-27.2057421880805,22.0945389044421,4.04631854726907));
#59810=CARTESIAN_POINT('Ctrl Pts',(-27.1615900298808,21.98821494112,4.05211628544009));
#59811=CARTESIAN_POINT('Ctrl Pts',(-27.1128588527272,21.8840216949444,4.05791402361112));
#59812=CARTESIAN_POINT('Ctrl Pts',(-27.0641311585802,21.779835895865,4.06371134739526));
#59813=CARTESIAN_POINT('Ctrl Pts',(-27.0108252750434,21.6777808932096,4.06950867117941));
#59814=CARTESIAN_POINT('Ctrl Pts',(-26.9531658491457,21.5782814482573,4.07530599496355));
#59815=CARTESIAN_POINT('Ctrl Pts',(-26.895495941529,21.4787639156254,4.08110437262427));
#59816=CARTESIAN_POINT('Ctrl Pts',(-26.8334711306767,21.3818032286698,4.08690275028499));
#59817=CARTESIAN_POINT('Ctrl Pts',(-26.7673606250504,21.2877971143075,4.09270112794572));
#59818=CARTESIAN_POINT('Ctrl Pts',(-26.7011810180815,21.1936927409977,4.0985055663025));
#59819=CARTESIAN_POINT('Ctrl Pts',(-26.6309074328281,21.1025494518367,4.10431000465928));
#59820=CARTESIAN_POINT('Ctrl Pts',(-26.5568508219523,21.0147337049021,4.11011444301607));
#59821=CARTESIAN_POINT('Ctrl Pts',(-26.4827528227106,20.9268688799686,4.11592212532658));
#59822=CARTESIAN_POINT('Ctrl Pts',(-26.4048678745775,20.8423356092517,4.1217298076371));
#59823=CARTESIAN_POINT('Ctrl Pts',(-26.3235440984385,20.7614637469662,4.12753748994761));
#59824=CARTESIAN_POINT('Ctrl Pts',(-26.2420916307683,20.6804639082844,4.13335436267654));
#59825=CARTESIAN_POINT('Ctrl Pts',(-26.1571897801108,20.6031373315479,4.13917123540548));
#59826=CARTESIAN_POINT('Ctrl Pts',(-26.0692202443632,20.5297739830978,4.14498810813441));
#59827=CARTESIAN_POINT('Ctrl Pts',(-26.0087143748169,20.4793143193849,4.14898898115839));
#59828=CARTESIAN_POINT('Ctrl Pts',(-25.9467579266626,20.4307286938456,4.15298985418237));
#59829=CARTESIAN_POINT('Ctrl Pts',(-25.8834825318848,20.3840992242546,4.15699072720635));
#59830=CARTESIAN_POINT('Ctrl Pts',(-25.7906098246731,20.31565863859,4.16286302417505));
#59831=CARTESIAN_POINT('Ctrl Pts',(-25.6945676280462,20.2511932106756,4.16873532114375));
#59832=CARTESIAN_POINT('Ctrl Pts',(-25.595730993464,20.1910105245688,4.17460761811246));
#59833=CARTESIAN_POINT('Ctrl Pts',(-25.4970224433104,20.1309058304433,4.18047230505067));
#59834=CARTESIAN_POINT('Ctrl Pts',(-25.3955270066242,20.0750730539903,4.18633699198889));
#59835=CARTESIAN_POINT('Ctrl Pts',(-25.2916513271279,20.023778480285,4.19220167892711));
#59836=CARTESIAN_POINT('Ctrl Pts',(-25.1878824772655,19.9725366598379,4.19806033440193));
#59837=CARTESIAN_POINT('Ctrl Pts',(-25.0817386220792,19.9258239406549,4.20391898987675));
#59838=CARTESIAN_POINT('Ctrl Pts',(-24.9736532258043,19.8838620091221,4.20977764535157));
#59839=CARTESIAN_POINT('Ctrl Pts',(-24.8613459187506,19.840261007584,4.21586514506947));
#59840=CARTESIAN_POINT('Ctrl Pts',(-24.7469426902543,19.8017897361575,4.22195264478738));
#59841=CARTESIAN_POINT('Ctrl Pts',(-24.6309557567804,19.7686431468835,4.22804014450528));
#59842=CARTESIAN_POINT('Ctrl Pts',(-24.5194583444578,19.7367795669036,4.23389201458867));
#59843=CARTESIAN_POINT('Ctrl Pts',(-24.40649798337,19.7098362515877,4.23974388467207));
#59844=CARTESIAN_POINT('Ctrl Pts',(-24.2925468457534,19.687936108702,4.24559575475546));
#59845=CARTESIAN_POINT('Ctrl Pts',(-24.1786130582335,19.6660393003121,4.25144673383843));
#59846=CARTESIAN_POINT('Ctrl Pts',(-24.0636891999744,19.6491842155817,4.25729771292141));
#59847=CARTESIAN_POINT('Ctrl Pts',(-23.9482580231877,19.6374427192013,4.26314869200438));
#59848=CARTESIAN_POINT('Ctrl Pts',(-23.8328164680277,19.6257001671474,4.26900019714666));
#59849=CARTESIAN_POINT('Ctrl Pts',(-23.7168679149511,19.6190721592409,4.27485170228894));
#59850=CARTESIAN_POINT('Ctrl Pts',(-23.6008999187749,19.6175786522348,4.28070320743123));
#59851=CARTESIAN_POINT('Ctrl Pts',(-23.4848934121511,19.6160846492677,4.28655665573101));
#59852=CARTESIAN_POINT('Ctrl Pts',(-23.368867862719,19.619728542918,4.2924101040308));
#59853=CARTESIAN_POINT('Ctrl Pts',(-23.2533097898436,19.6284781873365,4.29826355233058));
#59854=CARTESIAN_POINT('Ctrl Pts',(-23.1376203023466,19.6372377820006,4.30412365727212));
#59855=CARTESIAN_POINT('Ctrl Pts',(-23.0223997649561,19.6511146854975,4.30998376221366));
#59856=CARTESIAN_POINT('Ctrl Pts',(-22.908128648405,19.6700249715491,4.3158438671552));
#59857=CARTESIAN_POINT('Ctrl Pts',(-22.7937805774088,19.6889479924948,4.32170791851065));
#59858=CARTESIAN_POINT('Ctrl Pts',(-22.6803836038382,19.7129110602377,4.3275719698661));
#59859=CARTESIAN_POINT('Ctrl Pts',(-22.5684053876209,19.7417797162897,4.33343602122155));
#59860=CARTESIAN_POINT('Ctrl Pts',(-22.4562621378658,19.770690918978,4.33930871501812));
#59861=CARTESIAN_POINT('Ctrl Pts',(-22.345542212482,19.8045220190324,4.34518140881469));
#59862=CARTESIAN_POINT('Ctrl Pts',(-22.2366956600887,19.8430895537476,4.35105410261126));
#59863=CARTESIAN_POINT('Ctrl Pts',(-22.206895294824,19.8536486995965,4.35266194793459));
#59864=CARTESIAN_POINT('Ctrl Pts',(-22.177235220616,19.8645626045907,4.35426979325792));
#59865=CARTESIAN_POINT('Ctrl Pts',(-22.1477243593861,19.8758268995876,4.35587763858125));
#59866=CARTESIAN_POINT('Ctrl Pts',(-22.0399425109518,19.916967228452,4.36174993554996));
#59867=CARTESIAN_POINT('Ctrl Pts',(-21.9337917860359,19.9629228432228,4.36762223251866));
#59868=CARTESIAN_POINT('Ctrl Pts',(-21.82973369148,20.0135444690365,4.37349452948737));
#59869=CARTESIAN_POINT('Ctrl Pts',(-21.7258104479508,20.0641004932433,4.37935921642557));
#59870=CARTESIAN_POINT('Ctrl Pts',(-21.6239748101192,20.1193103244505,4.38522390336377));
#59871=CARTESIAN_POINT('Ctrl Pts',(-21.5246706162578,20.1789757848434,4.39108859030197));
#59872=CARTESIAN_POINT('Ctrl Pts',(-21.4254685505429,20.2385798830456,4.39694724577681));
#59873=CARTESIAN_POINT('Ctrl Pts',(-21.3287931026507,20.3026302843108,4.40280590125166));
#59874=CARTESIAN_POINT('Ctrl Pts',(-21.2350650868523,20.3708821387946,4.4086645567265));
#59875=CARTESIAN_POINT('Ctrl Pts',(-21.1376759722027,20.4417999708297,4.41475205644441));
#59876=CARTESIAN_POINT('Ctrl Pts',(-21.043469651172,20.5172539733303,4.42083955616231));
#59877=CARTESIAN_POINT('Ctrl Pts',(-20.9528870148963,20.596918589833,4.42692705588021));
#59878=CARTESIAN_POINT('Ctrl Pts',(-20.8658105723731,20.673499617779,4.4327789259636));
#59879=CARTESIAN_POINT('Ctrl Pts',(-20.7820828452387,20.7539710607026,4.438630796047));
#59880=CARTESIAN_POINT('Ctrl Pts',(-20.7020624669695,20.8380021090371,4.44448266613039));
#59881=CARTESIAN_POINT('Ctrl Pts',(-20.6220542725305,20.9220203628805,4.45033364521336));
#59882=CARTESIAN_POINT('Ctrl Pts',(-20.5457525895909,21.0095968452202,4.45618462429634));
#59883=CARTESIAN_POINT('Ctrl Pts',(-20.4734788271562,21.1003642544327,4.46203560337931));
#59884=CARTESIAN_POINT('Ctrl Pts',(-20.4011985666146,21.1911398245089,4.46788710852161));
#59885=CARTESIAN_POINT('Ctrl Pts',(-20.3329472040104,21.2851065683714,4.47373861366392));
#59886=CARTESIAN_POINT('Ctrl Pts',(-20.269005073342,21.3818650854435,4.47959011880622));
#59887=CARTESIAN_POINT('Ctrl Pts',(-20.2050417088844,21.4786557339123,4.48544356710597));
#59888=CARTESIAN_POINT('Ctrl Pts',(-20.1453906496107,21.578239654348,4.49129701540573));
#59889=CARTESIAN_POINT('Ctrl Pts',(-20.0902878350205,21.6801901536513,4.49715046370548));
#59890=CARTESIAN_POINT('Ctrl Pts',(-20.0351223565645,21.7822565928107,4.50301056864701));
#59891=CARTESIAN_POINT('Ctrl Pts',(-19.9845156433017,21.8866946187397,4.50887067358855));
#59892=CARTESIAN_POINT('Ctrl Pts',(-19.9386568014461,21.9930546376379,4.51473077853008));
#59893=CARTESIAN_POINT('Ctrl Pts',(-19.8927670765306,22.0994862833521,4.52059482988553));
#59894=CARTESIAN_POINT('Ctrl Pts',(-19.8516317360271,22.2078421138009,4.52645888124098));
#59895=CARTESIAN_POINT('Ctrl Pts',(-19.8153904477701,22.317655998328,4.53232293259642));
#59896=CARTESIAN_POINT('Ctrl Pts',(-19.7790957470887,22.4276317265999,4.53819562639299));
#59897=CARTESIAN_POINT('Ctrl Pts',(-19.7477096057703,22.5390694012931,4.54406832018956));
#59898=CARTESIAN_POINT('Ctrl Pts',(-19.7213209439203,22.6514912195832,4.54994101398612));
#59899=CARTESIAN_POINT('Ctrl Pts',(-19.7140961697342,22.6822704328438,4.55154885930946));
#59900=CARTESIAN_POINT('Ctrl Pts',(-19.7072456936328,22.7131233792419,4.5531567046328));
#59901=CARTESIAN_POINT('Ctrl Pts',(-19.7007706624597,22.7440401909085,4.55476454995614));
#59902=CARTESIAN_POINT('Ctrl Pts',(-19.6771220531203,22.8569569602004,4.56063684692485));
#59903=CARTESIAN_POINT('Ctrl Pts',(-19.658406316016,22.9711043040757,4.56650914389356));
#59904=CARTESIAN_POINT('Ctrl Pts',(-19.644747327712,23.0860132596933,4.57238144086227));
#59905=CARTESIAN_POINT('Ctrl Pts',(-19.6311060403721,23.2007733024299,4.57824612780046));
#59906=CARTESIAN_POINT('Ctrl Pts',(-19.6225085183239,23.3162925874392,4.58411081473865));
#59907=CARTESIAN_POINT('Ctrl Pts',(-19.6190279446485,23.4320905826255,4.58997550167683));
#59908=CARTESIAN_POINT('Ctrl Pts',(-19.6155509505254,23.5477694868228,4.59583415715163));
#59909=CARTESIAN_POINT('Ctrl Pts',(-19.6171804498143,23.6637261203512,4.60169281262643));
#59910=CARTESIAN_POINT('Ctrl Pts',(-19.6239379141862,23.7794740933833,4.60755146810123));
#59911=CARTESIAN_POINT('Ctrl Pts',(-19.6309593310684,23.899743284192,4.61363896781914));
#59912=CARTESIAN_POINT('Ctrl Pts',(-19.6435175391514,24.019786729766,4.61972646753705));
#59913=CARTESIAN_POINT('Ctrl Pts',(-19.6615769626702,24.1390575239252,4.62581396725495));
#59914=CARTESIAN_POINT('Ctrl Pts',(-19.6789373577603,24.2537116881154,4.63166583733836));
#59915=CARTESIAN_POINT('Ctrl Pts',(-19.7013809468752,24.3676514560851,4.63751770742176));
#59916=CARTESIAN_POINT('Ctrl Pts',(-19.7288232709736,24.4803962868786,4.64336957750517));
#59917=CARTESIAN_POINT('Ctrl Pts',(-19.7562614167287,24.5931239512464,4.64922055658814));
#59918=CARTESIAN_POINT('Ctrl Pts',(-19.788696686414,24.7046566386473,4.65507153567112));
#59919=CARTESIAN_POINT('Ctrl Pts',(-19.8259937982043,24.8145254001937,4.66092251475409));
#59920=CARTESIAN_POINT('Ctrl Pts',(-19.8632942633637,24.9244040399989,4.66677401989639));
#59921=CARTESIAN_POINT('Ctrl Pts',(-19.9054573067041,25.0326180650866,4.67262552503868));
#59922=CARTESIAN_POINT('Ctrl Pts',(-19.9522984382295,25.1387157328168,4.67847703018097));
#59923=CARTESIAN_POINT('Ctrl Pts',(-19.9991551246748,25.2448486332723,4.68433047848072));
#59924=CARTESIAN_POINT('Ctrl Pts',(-20.0506928214555,25.3488634009369,4.69018392678047));
#59925=CARTESIAN_POINT('Ctrl Pts',(-20.1066800798098,25.4503308902423,4.69603737508021));
#59926=CARTESIAN_POINT('Ctrl Pts',(-20.1627310078344,25.5519137701165,4.70189748002175));
#59927=CARTESIAN_POINT('Ctrl Pts',(-20.223241397446,25.6509432275333,4.70775758496329));
#59928=CARTESIAN_POINT('Ctrl Pts',(-20.2879352177625,25.7470171397533,4.71361768990483));
#59929=CARTESIAN_POINT('Ctrl Pts',(-20.352672605318,25.8431557517404,4.71948174126029));
#59930=CARTESIAN_POINT('Ctrl Pts',(-20.4215987881028,25.9363345237726,4.72534579261576));
#59931=CARTESIAN_POINT('Ctrl Pts',(-20.4943970989599,26.0261839875767,4.73120984397122));
#59932=CARTESIAN_POINT('Ctrl Pts',(-20.5673026999952,26.1161658715545,4.73708253776779));
#59933=CARTESIAN_POINT('Ctrl Pts',(-20.6440915455078,26.2028083462002,4.74295523156437));
#59934=CARTESIAN_POINT('Ctrl Pts',(-20.7244097170516,26.2857783288551,4.74882792536094));
#59935=CARTESIAN_POINT('Ctrl Pts',(-20.7463994888618,26.3084941221882,4.7504357706843));
#59936=CARTESIAN_POINT('Ctrl Pts',(-20.7686536175801,26.330934868149,4.75204361600766));
#59937=CARTESIAN_POINT('Ctrl Pts',(-20.7911644211204,26.3530942678773,4.75365146133102));
#59938=CARTESIAN_POINT('Ctrl Pts',(-20.8733801177873,26.4340265403806,4.75952375829973));
#59939=CARTESIAN_POINT('Ctrl Pts',(-20.9592975440606,26.5114738824377,4.76539605526844));
#59940=CARTESIAN_POINT('Ctrl Pts',(-21.0485891141686,26.5850785803194,4.77126835223715));
#59941=CARTESIAN_POINT('Ctrl Pts',(-21.137764969493,26.6585878923581,4.77713303917535));
#59942=CARTESIAN_POINT('Ctrl Pts',(-21.2303059570408,26.7282642026665,4.78299772611355));
#59943=CARTESIAN_POINT('Ctrl Pts',(-21.3258473556551,26.7937861931213,4.78886241305175));
#59944=CARTESIAN_POINT('Ctrl Pts',(-21.4212904959224,26.8592407983109,4.79472106852659));
#59945=CARTESIAN_POINT('Ctrl Pts',(-21.5197275707047,26.9205493493921,4.80057972400143));
#59946=CARTESIAN_POINT('Ctrl Pts',(-21.6207609784277,26.9774308675666,4.80643837947628));
#59947=CARTESIAN_POINT('Ctrl Pts',(-21.725740840045,27.0365342279414,4.81252587919418));
#59948=CARTESIAN_POINT('Ctrl Pts',(-21.833523648774,27.0908573681119,4.81861337891208));
#59949=CARTESIAN_POINT('Ctrl Pts',(-21.9436300530602,27.1401345925909,4.82470087862998));
#59950=CARTESIAN_POINT('Ctrl Pts',(-22.0494745545946,27.1875044372043,4.83055274871338));
#59951=CARTESIAN_POINT('Ctrl Pts',(-22.1574657044648,27.2302115439549,4.83640461879677));
#59952=CARTESIAN_POINT('Ctrl Pts',(-22.2671535618097,27.2680672168932,4.84225648888017));
#59953=CARTESIAN_POINT('Ctrl Pts',(-22.3768247181811,27.3059171259611,4.84810746796314));
#59954=CARTESIAN_POINT('Ctrl Pts',(-22.488191677708,27.3389169351142,4.85395844704612));
#59955=CARTESIAN_POINT('Ctrl Pts',(-22.6007867802616,27.3669269724681,4.85980942612909));
#59956=CARTESIAN_POINT('Ctrl Pts',(-22.7133920061983,27.3949395281938,4.86566093127138));
#59957=CARTESIAN_POINT('Ctrl Pts',(-22.8272251934898,27.4179613204876,4.87151243641367));
#59958=CARTESIAN_POINT('Ctrl Pts',(-22.9418065588099,27.4359033778307,4.87736394155595));
#59959=CARTESIAN_POINT('Ctrl Pts',(-23.0564259741077,27.4538513933405,4.88321738985575));
#59960=CARTESIAN_POINT('Ctrl Pts',(-23.1717936532784,27.4667162557484,4.88907083815554));
#59961=CARTESIAN_POINT('Ctrl Pts',(-23.2874234410873,27.4744607154086,4.89492428645533));
#59962=CARTESIAN_POINT('Ctrl Pts',(-23.4031847250729,27.482213982201,4.90078439139687));
#59963=CARTESIAN_POINT('Ctrl Pts',(-23.5192082999409,27.4848351960528,4.90664449633841));
#59964=CARTESIAN_POINT('Ctrl Pts',(-23.6350066466901,27.4823392219887,4.91250460127995));
#59965=CARTESIAN_POINT('Ctrl Pts',(-23.7508829763782,27.4798415670423,4.91836865263539));
#59966=CARTESIAN_POINT('Ctrl Pts',(-23.8665333644483,27.4722198894168,4.92423270399083));
#59967=CARTESIAN_POINT('Ctrl Pts',(-23.9814757990205,27.4595408932399,4.93009675534627));
#59968=CARTESIAN_POINT('Ctrl Pts',(-24.0965876357965,27.4468432107535,4.93596944914284));
#59969=CARTESIAN_POINT('Ctrl Pts',(-24.2109890297344,27.4290733972227,4.9418421429394));
#59970=CARTESIAN_POINT('Ctrl Pts',(-24.3242084448811,27.4063491648769,4.94771483673597));
#59971=CARTESIAN_POINT('Ctrl Pts',(-24.3552060268187,27.4001276501906,4.9493226820593));
#59972=CARTESIAN_POINT('Ctrl Pts',(-24.386115102903,27.3935350528374,4.95093052738262));
#59973=CARTESIAN_POINT('Ctrl Pts',(-24.4169262213039,27.3865744310841,4.95253837270595));
#59974=CARTESIAN_POINT('Ctrl Pts',(-24.5294569694817,27.3611523102935,4.95841066967465));
#59975=CARTESIAN_POINT('Ctrl Pts',(-24.6410567289838,27.3307321096338,4.96428296664336));
#59976=CARTESIAN_POINT('Ctrl Pts',(-24.751247475251,27.2953960730756,4.97015526361206));
#59977=CARTESIAN_POINT('Ctrl Pts',(-24.8612954230623,27.2601058292145,4.97601995055026));
#59978=CARTESIAN_POINT('Ctrl Pts',(-24.9699375988315,27.2199125432252,4.98188463748845));
#59979=CARTESIAN_POINT('Ctrl Pts',(-25.0767065249837,27.1749493750689,4.98774932442665));
#59980=CARTESIAN_POINT('Ctrl Pts',(-25.1833656459794,27.1300324487162,4.99360797990148));
#59981=CARTESIAN_POINT('Ctrl Pts',(-25.2881549706174,27.0803555570138,4.99946663537631));
#59982=CARTESIAN_POINT('Ctrl Pts',(-25.390623186214,27.0261013278852,5.00532529085113));
#59983=CARTESIAN_POINT('Ctrl Pts',(-25.4970939005645,26.9697278807804,5.01141279056904));
#59984=CARTESIAN_POINT('Ctrl Pts',(-25.6010580471928,26.9084123555736,5.01750029028694));
#59985=CARTESIAN_POINT('Ctrl Pts',(-25.7020329821909,26.8424144190959,5.02358779000484));
#59986=CARTESIAN_POINT('Ctrl Pts',(-25.7990994673934,26.7789710732336,5.02943966008824));
#59987=CARTESIAN_POINT('Ctrl Pts',(-25.8934034674278,26.7112013086271,5.03529153017163));
#59988=CARTESIAN_POINT('Ctrl Pts',(-25.9845430171159,26.6393816699119,5.04114340025503));
#59989=CARTESIAN_POINT('Ctrl Pts',(-26.075668689979,26.5675729663896,5.046994379338));
#59990=CARTESIAN_POINT('Ctrl Pts',(-26.1636305459032,26.4917158706057,5.05284535842097));
#59991=CARTESIAN_POINT('Ctrl Pts',(-26.2480582864638,26.4121283342985,5.05869633750394));
#59992=CARTESIAN_POINT('Ctrl Pts',(-26.3324936178905,26.3325336423061,5.06454784264622));
#59993=CARTESIAN_POINT('Ctrl Pts',(-26.4133939014749,26.2492081266143,5.0703993477885));
#59994=CARTESIAN_POINT('Ctrl Pts',(-26.4904249407582,26.1625073441079,5.07625085293078));
#59995=CARTESIAN_POINT('Ctrl Pts',(-26.5674815603729,26.0757777701589,5.08210430123054));
#59996=CARTESIAN_POINT('Ctrl Pts',(-26.640666106341,25.9856710095174,5.0879577495303));
#59997=CARTESIAN_POINT('Ctrl Pts',(-26.7096844523967,25.8925759377264,5.09381119783007));
#59998=CARTESIAN_POINT('Ctrl Pts',(-26.7787812872988,25.7993749966237,5.09967130277159));
#59999=CARTESIAN_POINT('Ctrl Pts',(-26.8437022192963,25.7031792936232,5.10553140771312));
#60000=CARTESIAN_POINT('Ctrl Pts',(-26.9041962298964,25.6044070218165,5.11139151265465));
#60001=CARTESIAN_POINT('Ctrl Pts',(-26.9647309794266,25.5055682330665,5.1172555640101));
#60002=CARTESIAN_POINT('Ctrl Pts',(-27.0208326716819,25.4041497813098,5.12311961536555));
#60003=CARTESIAN_POINT('Ctrl Pts',(-27.072296878109,25.3005932476371,5.128983666721));
#60004=CARTESIAN_POINT('Ctrl Pts',(-27.1238369325031,25.1968840923057,5.13485636051757));
#60005=CARTESIAN_POINT('Ctrl Pts',(-27.1707256934761,25.0910309426017,5.14072905431413));
#60006=CARTESIAN_POINT('Ctrl Pts',(-27.2128073091294,24.9834941380839,5.1466017481107));
#60007=CARTESIAN_POINT('Ctrl Pts',(-27.2243285515562,24.954052359877,5.14820959343408));
#60008=CARTESIAN_POINT('Ctrl Pts',(-27.2354897547434,24.9244844572167,5.14981743875746));
#60009=CARTESIAN_POINT('Ctrl Pts',(-27.2462883825474,24.894800035209,5.15142528408085));
#60010=CARTESIAN_POINT('Ctrl Pts',(-27.2919542468375,24.7692688277693,5.15822463374541));
#60011=CARTESIAN_POINT('Ctrl Pts',(-27.3312583294848,24.6413065928319,5.16502398340998));
#60012=CARTESIAN_POINT('Ctrl Pts',(-27.3639717707758,24.5115196982296,5.17182333307454));
#60013=CARTESIAN_POINT('Ctrl Pts',(-27.3965467409697,24.382282172112,5.17859390211042));
#60014=CARTESIAN_POINT('Ctrl Pts',(-27.4225866449772,24.2512355293688,5.1853644711463));
#60015=CARTESIAN_POINT('Ctrl Pts',(-27.4419122083623,24.119000244653,5.19213504018218));
#60016=CARTESIAN_POINT('Ctrl Pts',(-27.461088734335,23.9877847493355,5.19885339505647));
#60017=CARTESIAN_POINT('Ctrl Pts',(-27.4736539935025,23.8553990195052,5.20557174993076));
#60018=CARTESIAN_POINT('Ctrl Pts',(-27.4794802654773,23.7224687216122,5.21229010480506));
#60019=CARTESIAN_POINT('Ctrl Pts',(-27.4819507716076,23.6661024693548,5.21513887962616));
#60020=CARTESIAN_POINT('Ctrl Pts',(-27.4832101997752,23.6096385311086,5.21798765444727));
#60021=CARTESIAN_POINT('Ctrl Pts',(-27.4832514823194,23.5531255756082,5.22083642926838));
#60022=CARTESIAN_POINT('',(-27.4785911626596,23.547629167803,6.47083647796516));
#60023=CARTESIAN_POINT('Ctrl Pts',(-27.4790683860637,23.5531215548671,5.22083647796515));
#60024=CARTESIAN_POINT('Ctrl Pts',(-27.473319408008,22.6978634849193,5.263995050462));
#60025=CARTESIAN_POINT('Ctrl Pts',(-26.7776474908277,20.520334858285,5.3734492600839));
#60026=CARTESIAN_POINT('Ctrl Pts',(-23.1797246374427,18.9130702070832,5.54919910683057));
#60027=CARTESIAN_POINT('Ctrl Pts',(-19.4486272035729,21.3553902353711,5.7480860182055));
#60028=CARTESIAN_POINT('Ctrl Pts',(-19.4865756857664,25.8146026203464,5.94697292958035));
#60029=CARTESIAN_POINT('Ctrl Pts',(-23.2586986463879,28.1930692590768,6.14585984095524));
#60030=CARTESIAN_POINT('Ctrl Pts',(-26.8058194983606,26.5355178218322,6.32048102375024));
#60031=CARTESIAN_POINT('Ctrl Pts',(-27.473510843006,24.3807749536279,6.42880656942016));
#60032=CARTESIAN_POINT('Ctrl Pts',(-27.4785911626596,23.547629167803,6.47083647796516));
#60033=CARTESIAN_POINT('',(-27.4886577079825,23.5483711242969,7.72083647796516));
#60034=CARTESIAN_POINT('Ctrl Pts',(-27.4785911626596,23.547629167803,6.47083647796516));
#60035=CARTESIAN_POINT('Ctrl Pts',(-27.4815242563085,23.0666171883284,6.49510220654513));
#60036=CARTESIAN_POINT('Ctrl Pts',(-27.1765185624428,21.2750381511308,6.58566357225004));
#60037=CARTESIAN_POINT('Ctrl Pts',(-24.4979820906171,18.99585251465,6.74252057507997));
#60038=CARTESIAN_POINT('Ctrl Pts',(-20.2308473862112,20.2910654685983,6.94140748645481));
#60039=CARTESIAN_POINT('Ctrl Pts',(-19.0139645713602,24.5811950000388,7.14029439782973));
#60040=CARTESIAN_POINT('Ctrl Pts',(-21.9655457782616,27.9239758125756,7.33918130920452));
#60041=CARTESIAN_POINT('Ctrl Pts',(-26.2542626229903,27.2659458526094,7.53269533591654));
#60042=CARTESIAN_POINT('Ctrl Pts',(-27.4815868075466,24.7481226885398,7.65991372550328));
#60043=CARTESIAN_POINT('Ctrl Pts',(-27.4886577079825,23.5483711242969,7.72083647796516));
#60044=CARTESIAN_POINT('',(-27.4832509407115,23.5537901392572,8.97083647796516));
#60045=CARTESIAN_POINT('Ctrl Pts',(-27.4886577079825,23.5483711242969,7.72083647796516));
#60046=CARTESIAN_POINT('Ctrl Pts',(-27.489281303125,23.4425629242642,7.72620936262824));
#60047=CARTESIAN_POINT('Ctrl Pts',(-27.4373560099309,22.0318165836772,7.79787788441659));
#60048=CARTESIAN_POINT('Ctrl Pts',(-25.739834537459,19.4458059828765,7.93584204332904));
#60049=CARTESIAN_POINT('Ctrl Pts',(-21.2806746818376,19.4894930934159,8.1347289547043));
#60050=CARTESIAN_POINT('Ctrl Pts',(-18.9070644417657,23.2646738321175,8.33361586607897));
#60051=CARTESIAN_POINT('Ctrl Pts',(-20.8001503789075,27.3022771826442,8.53250277745392));
#60052=CARTESIAN_POINT('Ctrl Pts',(-25.220347024252,27.8920879981818,8.73138968882892));
#60053=CARTESIAN_POINT('Ctrl Pts',(-27.3401802964048,25.3943193256145,8.87750092233257));
#60054=CARTESIAN_POINT('Ctrl Pts',(-27.4868802877149,23.8207898070215,8.95731651871135));
#60055=CARTESIAN_POINT('Ctrl Pts',(-27.4844023746644,23.5537911749356,8.97083647796516));
#60056=CARTESIAN_POINT('',(-27.4832525242572,23.5504943982642,10.220836477917));
#60057=CARTESIAN_POINT('Ctrl Pts',(-27.4832509407115,23.5537901392572,8.97083647796516));
#60058=CARTESIAN_POINT('Ctrl Pts',(-27.4833535323691,23.4397320310741,8.97661376058633));
#60059=CARTESIAN_POINT('Ctrl Pts',(-27.4784903597999,23.3255145710099,8.9823910432075));
#60060=CARTESIAN_POINT('Ctrl Pts',(-27.4686465801482,23.2116124852729,8.98816832582867));
#60061=CARTESIAN_POINT('Ctrl Pts',(-27.458636643878,23.0957878061744,8.99404312523492));
#60062=CARTESIAN_POINT('Ctrl Pts',(-27.4434763704664,22.9802896886087,8.99991792464117));
#60063=CARTESIAN_POINT('Ctrl Pts',(-27.4232054851861,22.8656180160302,9.00579272404742));
#60064=CARTESIAN_POINT('Ctrl Pts',(-27.403298315435,22.7530038691839,9.01156211336696));
#60065=CARTESIAN_POINT('Ctrl Pts',(-27.3784624844721,22.641187194019,9.0173315026865));
#60066=CARTESIAN_POINT('Ctrl Pts',(-27.3487878283232,22.5306356427288,9.02310089200604));
#60067=CARTESIAN_POINT('Ctrl Pts',(-27.3191196006254,22.420108040334,9.02886903149688));
#60068=CARTESIAN_POINT('Ctrl Pts',(-27.2846147411839,22.3108454287445,9.03463717098771));
#60069=CARTESIAN_POINT('Ctrl Pts',(-27.2454137135604,22.2033030745768,9.04040531047856));
#60070=CARTESIAN_POINT('Ctrl Pts',(-27.2062110518577,22.0957562375486,9.04617369041201));
#60071=CARTESIAN_POINT('Ctrl Pts',(-27.1623119798,21.989930200693,9.05194207034546));
#60072=CARTESIAN_POINT('Ctrl Pts',(-27.1139058262283,21.886262088105,9.05771045027891));
#60073=CARTESIAN_POINT('Ctrl Pts',(-27.063938476956,21.7792504706168,9.06366487205388));
#60074=CARTESIAN_POINT('Ctrl Pts',(-27.0091685897512,21.6745387763222,9.06961929382886));
#60075=CARTESIAN_POINT('Ctrl Pts',(-26.9498560258286,21.5725809000351,9.07557371560384));
#60076=CARTESIAN_POINT('Ctrl Pts',(-26.8923154352202,21.4736690332947,9.0813502479775));
#60077=CARTESIAN_POINT('Ctrl Pts',(-26.830500027148,21.3773491085231,9.08712678035116));
#60078=CARTESIAN_POINT('Ctrl Pts',(-26.7646907147518,21.2840053767481,9.09290331272483));
#60079=CARTESIAN_POINT('Ctrl Pts',(-26.6958414871195,21.1863498382988,9.09894667920047));
#60080=CARTESIAN_POINT('Ctrl Pts',(-26.6226208652533,21.0919524606182,9.1049900456761));
#60081=CARTESIAN_POINT('Ctrl Pts',(-26.5453959638536,21.0012125514679,9.11103341215174));
#60082=CARTESIAN_POINT('Ctrl Pts',(-26.468171062454,20.9104726423175,9.11707677862737));
#60083=CARTESIAN_POINT('Ctrl Pts',(-26.3869422980837,20.8233905312141,9.123120145103));
#60084=CARTESIAN_POINT('Ctrl Pts',(-26.302117430245,20.7403186214173,9.12916351157864));
#60085=CARTESIAN_POINT('Ctrl Pts',(-26.2196936989872,20.6595982272378,9.13503580854734));
#60086=CARTESIAN_POINT('Ctrl Pts',(-26.1335772200464,20.58237227963,9.14090810551604));
#60087=CARTESIAN_POINT('Ctrl Pts',(-26.0440964988077,20.508997647984,9.14678040248474));
#60088=CARTESIAN_POINT('Ctrl Pts',(-25.9547317374774,20.4357181040332,9.15264508942294));
#60089=CARTESIAN_POINT('Ctrl Pts',(-25.8620117206126,20.3662802104368,9.15850977636114));
#60090=CARTESIAN_POINT('Ctrl Pts',(-25.7663019951844,20.3010043455187,9.16437446329934));
#60091=CARTESIAN_POINT('Ctrl Pts',(-25.6706907012169,20.2357956127412,9.17023311877418));
#60092=CARTESIAN_POINT('Ctrl Pts',(-25.5720961539414,20.1747406262546,9.17609177424902));
#60093=CARTESIAN_POINT('Ctrl Pts',(-25.4709166768101,20.1181193405628,9.18195042972386));
#60094=CARTESIAN_POINT('Ctrl Pts',(-25.3657850401848,20.0592863775806,9.18803792944176));
#60095=CARTESIAN_POINT('Ctrl Pts',(-25.2578627692656,20.0052408333131,9.19412542915967));
#60096=CARTESIAN_POINT('Ctrl Pts',(-25.1476298978777,19.9562471685924,9.20021292887757));
#60097=CARTESIAN_POINT('Ctrl Pts',(-25.0416638244199,19.9091499079532,9.20606479896096));
#60098=CARTESIAN_POINT('Ctrl Pts',(-24.9335631108894,19.8667208948667,9.21191666904436));
#60099=CARTESIAN_POINT('Ctrl Pts',(-24.8237781823305,19.8291476665807,9.21776853912775));
#60100=CARTESIAN_POINT('Ctrl Pts',(-24.714009969525,19.7915801591603,9.22361951821072));
#60101=CARTESIAN_POINT('Ctrl Pts',(-24.6025584425741,19.7588671003197,9.22947049729369));
#60102=CARTESIAN_POINT('Ctrl Pts',(-24.4898916195508,19.7311469577971,9.23532147637667));
#60103=CARTESIAN_POINT('Ctrl Pts',(-24.3772146666962,19.703424322967,9.24117298151895));
#60104=CARTESIAN_POINT('Ctrl Pts',(-24.2633226019928,19.6806955956168,9.24702448666124));
#60105=CARTESIAN_POINT('Ctrl Pts',(-24.1486954361764,19.6630485120838,9.25287599180353));
#60106=CARTESIAN_POINT('Ctrl Pts',(-24.0340302051732,19.6453955683385,9.25872944010331));
#60107=CARTESIAN_POINT('Ctrl Pts',(-23.9186297960107,19.6328276867713,9.26458288840309));
#60108=CARTESIAN_POINT('Ctrl Pts',(-23.8029804581881,19.6253808656177,9.27043633670287));
#60109=CARTESIAN_POINT('Ctrl Pts',(-23.6871996019558,19.6179255758114,9.27629644164441));
#60110=CARTESIAN_POINT('Ctrl Pts',(-23.5711696648056,19.615602997042,9.28215654658595));
#60111=CARTESIAN_POINT('Ctrl Pts',(-23.4553781258636,19.618397009537,9.28801665152749));
#60112=CARTESIAN_POINT('Ctrl Pts',(-23.3395086085669,19.6211929036245,9.29388070288295));
#60113=CARTESIAN_POINT('Ctrl Pts',(-23.2238782205669,19.6291122218805,9.29974475423841));
#60114=CARTESIAN_POINT('Ctrl Pts',(-23.1089688004609,19.6420870197757,9.30560880559387));
#60115=CARTESIAN_POINT('Ctrl Pts',(-22.993890026808,19.655080939933,9.31148149939044));
#60116=CARTESIAN_POINT('Ctrl Pts',(-22.8795347485061,19.6731451457662,9.31735419318701));
#60117=CARTESIAN_POINT('Ctrl Pts',(-22.7663741969737,19.6961607117766,9.32322688698358));
#60118=CARTESIAN_POINT('Ctrl Pts',(-22.7353927309093,19.7024619887468,9.32483473230689));
#60119=CARTESIAN_POINT('Ctrl Pts',(-22.7045007255135,19.7091341193546,9.32644257763021));
#60120=CARTESIAN_POINT('Ctrl Pts',(-22.6737076247133,19.7161740210158,9.32805042295352));
#60121=CARTESIAN_POINT('Ctrl Pts',(-22.5612426818085,19.7418856940143,9.33392271992222));
#60122=CARTESIAN_POINT('Ctrl Pts',(-22.4497215887658,19.7725930341085,9.33979501689092));
#60123=CARTESIAN_POINT('Ctrl Pts',(-22.3396221568778,19.8082125672401,9.34566731385962));
#60124=CARTESIAN_POINT('Ctrl Pts',(-22.2296654051097,19.8437859402855,9.35153200079782));
#60125=CARTESIAN_POINT('Ctrl Pts',(-22.1211270403851,19.884258720983,9.35739668773601));
#60126=CARTESIAN_POINT('Ctrl Pts',(-22.0144741959979,19.9294965465986,9.3632613746742));
#60127=CARTESIAN_POINT('Ctrl Pts',(-21.9079310373844,19.9746878479425,9.36912003014902));
#60128=CARTESIAN_POINT('Ctrl Pts',(-21.8032699203359,20.0246342863084,9.37497868562384));
#60129=CARTESIAN_POINT('Ctrl Pts',(-21.7009416859858,20.0791520727698,9.38083734109866));
#60130=CARTESIAN_POINT('Ctrl Pts',(-21.5946164206724,20.1357993719891,9.38692484081657));
#60131=CARTESIAN_POINT('Ctrl Pts',(-21.4908104349089,20.1973822814301,9.39301234053447));
#60132=CARTESIAN_POINT('Ctrl Pts',(-21.3900057026632,20.2636398928727,9.39909984025238));
#60133=CARTESIAN_POINT('Ctrl Pts',(-21.2931028321534,20.3273328624275,9.40495171033577));
#60134=CARTESIAN_POINT('Ctrl Pts',(-21.1989735731815,20.3953451261943,9.41080358041916));
#60135=CARTESIAN_POINT('Ctrl Pts',(-21.108019177812,20.4673991058587,9.41665545050255));
#60136=CARTESIAN_POINT('Ctrl Pts',(-21.0170786310761,20.5394421146497,9.42250642958552));
#60137=CARTESIAN_POINT('Ctrl Pts',(-20.9293123107232,20.6155253591264,9.42835740866849));
#60138=CARTESIAN_POINT('Ctrl Pts',(-20.8450896955939,20.6953299355138,9.43420838775146));
#60139=CARTESIAN_POINT('Ctrl Pts',(-20.7608595080411,20.7751416871005,9.44005989289374));
#60140=CARTESIAN_POINT('Ctrl Pts',(-20.6801739591736,20.8586751513727,9.44591139803602));
#60141=CARTESIAN_POINT('Ctrl Pts',(-20.603366329196,20.9455739124543,9.4517629031783));
#60142=CARTESIAN_POINT('Ctrl Pts',(-20.5265331930761,21.0325015307231,9.45761635147808));
#60143=CARTESIAN_POINT('Ctrl Pts',(-20.4535808101237,21.1227963583906,9.46346979977786));
#60144=CARTESIAN_POINT('Ctrl Pts',(-20.3848023047259,21.2160687641672,9.46932324807764));
#60145=CARTESIAN_POINT('Ctrl Pts',(-20.3159455832326,21.3094472409228,9.47518335301919));
#60146=CARTESIAN_POINT('Ctrl Pts',(-20.2512724588572,21.4058097215403,9.48104345796073));
#60147=CARTESIAN_POINT('Ctrl Pts',(-20.1910328728978,21.5047373682314,9.48690356290228));
#60148=CARTESIAN_POINT('Ctrl Pts',(-20.1307527193476,21.603731636501,9.49276761425773));
#60149=CARTESIAN_POINT('Ctrl Pts',(-20.0749122480346,21.7052941492416,9.49863166561318));
#60150=CARTESIAN_POINT('Ctrl Pts',(-20.0237147502748,21.8089828006584,9.50449571696863));
#60151=CARTESIAN_POINT('Ctrl Pts',(-19.9724417976234,21.9128242684489,9.51036841076519));
#60152=CARTESIAN_POINT('Ctrl Pts',(-19.9258256412901,22.0187977518141,9.51624110456176));
#60153=CARTESIAN_POINT('Ctrl Pts',(-19.8840209478159,22.1264425115816,9.52211379835832));
#60154=CARTESIAN_POINT('Ctrl Pts',(-19.8725755220495,22.1559138461296,9.52372164368168));
#60155=CARTESIAN_POINT('Ctrl Pts',(-19.8614904589547,22.1855103780289,9.52532948900504));
#60156=CARTESIAN_POINT('Ctrl Pts',(-19.8507682699444,22.2152224956778,9.52693733432841));
#60157=CARTESIAN_POINT('Ctrl Pts',(-19.8116078624674,22.3237393883593,9.53280963129712));
#60158=CARTESIAN_POINT('Ctrl Pts',(-19.7771605843996,22.4341625741623,9.53868192826584));
#60159=CARTESIAN_POINT('Ctrl Pts',(-19.7476144848749,22.5460449411623,9.54455422523456));
#60160=CARTESIAN_POINT('Ctrl Pts',(-19.7181066747487,22.6577823174997,9.55041891217275));
#60161=CARTESIAN_POINT('Ctrl Pts',(-19.6934875168102,22.770974718556,9.55628359911094));
#60162=CARTESIAN_POINT('Ctrl Pts',(-19.6738964747858,22.8851565084995,9.56214828604914));
#60163=CARTESIAN_POINT('Ctrl Pts',(-19.6543255809215,22.9992208696208,9.56800694152399));
#60164=CARTESIAN_POINT('Ctrl Pts',(-19.6397725868679,23.114272190741,9.57386559699884));
#60165=CARTESIAN_POINT('Ctrl Pts',(-19.6303265666629,23.2298318259442,9.5797242524737));
#60166=CARTESIAN_POINT('Ctrl Pts',(-19.6205115765887,23.3499053222813,9.5858117521916));
#60167=CARTESIAN_POINT('Ctrl Pts',(-19.6162107756016,23.4705272130242,9.5918992519095));
#60168=CARTESIAN_POINT('Ctrl Pts',(-19.6174651846001,23.5911509734333,9.5979867516274));
#60169=CARTESIAN_POINT('Ctrl Pts',(-19.6186710390282,23.7071057344349,9.60383862171081));
#60170=CARTESIAN_POINT('Ctrl Pts',(-19.6250100427651,23.8230617711427,9.60969049179422));
#60171=CARTESIAN_POINT('Ctrl Pts',(-19.6364655582687,23.9385314606164,9.61554236187763));
#60172=CARTESIAN_POINT('Ctrl Pts',(-19.6479193295659,24.0539835687796,9.6213933409606));
#60173=CARTESIAN_POINT('Ctrl Pts',(-19.6644880228585,24.1689490656949,9.62724432004356));
#60174=CARTESIAN_POINT('Ctrl Pts',(-19.6861030580268,24.2829447216045,9.63309529912653));
#60175=CARTESIAN_POINT('Ctrl Pts',(-19.7077200365947,24.3969506268206,9.63894680426882));
#60176=CARTESIAN_POINT('Ctrl Pts',(-19.7343841819661,24.5099861115191,9.64479830941112));
#60177=CARTESIAN_POINT('Ctrl Pts',(-19.7659757875636,24.6215781235813,9.65064981455341));
#60178=CARTESIAN_POINT('Ctrl Pts',(-19.7975778840457,24.7332071929219,9.65650326285319));
#60179=CARTESIAN_POINT('Ctrl Pts',(-19.8341105818946,24.8433914389366,9.66235671115298));
#60180=CARTESIAN_POINT('Ctrl Pts',(-19.8754045239268,24.9516736389307,9.66821015945276));
#60181=CARTESIAN_POINT('Ctrl Pts',(-19.9167454261378,25.0600789792991,9.67407026439431));
#60182=CARTESIAN_POINT('Ctrl Pts',(-19.9628582324617,25.1665775698071,9.67993036933586));
#60183=CARTESIAN_POINT('Ctrl Pts',(-20.0135256715073,25.2707327310666,9.68579047427741));
#60184=CARTESIAN_POINT('Ctrl Pts',(-20.0642272319021,25.3749580343087,9.69165452563288));
#60185=CARTESIAN_POINT('Ctrl Pts',(-20.1194893359217,25.4768364034066,9.69751857698835));
#60186=CARTESIAN_POINT('Ctrl Pts',(-20.1790499201176,25.5759578290411,9.70338262834383));
#60187=CARTESIAN_POINT('Ctrl Pts',(-20.2386982847252,25.6752253398705,9.70925532214042));
#60188=CARTESIAN_POINT('Ctrl Pts',(-20.3026575456328,25.7717274546252,9.71512801593701));
#60189=CARTESIAN_POINT('Ctrl Pts',(-20.3706236790665,25.8650850006944,9.7210007097336));
#60190=CARTESIAN_POINT('Ctrl Pts',(-20.389231669465,25.8906447351257,9.72260855505684));
#60191=CARTESIAN_POINT('Ctrl Pts',(-20.4081397817965,25.915968964871,9.72421640038009));
#60192=CARTESIAN_POINT('Ctrl Pts',(-20.4273412871845,25.9410503815583,9.72582424570333));
#60193=CARTESIAN_POINT('Ctrl Pts',(-20.4974705093515,26.0326546702633,9.73169654267202));
#60194=CARTESIAN_POINT('Ctrl Pts',(-20.5717511741554,26.121324156364,9.73756883964072));
#60195=CARTESIAN_POINT('Ctrl Pts',(-20.6499087673609,26.2066589480193,9.74344113660941));
#60196=CARTESIAN_POINT('Ctrl Pts',(-20.7279650745329,26.2918831525619,9.7493058235476));
#60197=CARTESIAN_POINT('Ctrl Pts',(-20.8098880421657,26.3737809545392,9.7551705104858));
#60198=CARTESIAN_POINT('Ctrl Pts',(-20.8953613090781,26.451983324872,9.761035197424));
#60199=CARTESIAN_POINT('Ctrl Pts',(-20.980746672086,26.5301052689622,9.7668938528988));
#60200=CARTESIAN_POINT('Ctrl Pts',(-21.069674768672,26.6045390634698,9.77275250837361));
#60201=CARTESIAN_POINT('Ctrl Pts',(-21.1617910542897,26.6749510405035,9.77861116384841));
#60202=CARTESIAN_POINT('Ctrl Pts',(-21.2575054831589,26.7481133713783,9.78469866356632));
#60203=CARTESIAN_POINT('Ctrl Pts',(-21.3566619384073,26.8169329528803,9.79078616328422));
#60204=CARTESIAN_POINT('Ctrl Pts',(-21.4588227931366,26.8810798536485,9.79687366300213));
#60205=CARTESIAN_POINT('Ctrl Pts',(-21.5570292945226,26.9427438120784,9.80272553308551));
#60206=CARTESIAN_POINT('Ctrl Pts',(-21.6580115539928,27.000089855443,9.8085774031689));
#60207=CARTESIAN_POINT('Ctrl Pts',(-21.761350332889,27.0528684003144,9.81442927325229));
#60208=CARTESIAN_POINT('Ctrl Pts',(-21.8646733775168,27.1056389091726,9.82028025233526));
#60209=CARTESIAN_POINT('Ctrl Pts',(-21.9703518601126,27.1538431143281,9.82613123141824));
#60210=CARTESIAN_POINT('Ctrl Pts',(-22.0779421609116,27.1972775072168,9.83198221050121));
#60211=CARTESIAN_POINT('Ctrl Pts',(-22.1855421351137,27.2407158052754,9.8378337156435));
#60212=CARTESIAN_POINT('Ctrl Pts',(-22.2950538858743,27.2793832837907,9.84368522078579));
#60213=CARTESIAN_POINT('Ctrl Pts',(-22.4060147200292,27.3131249491907,9.84953672592807));
#60214=CARTESIAN_POINT('Ctrl Pts',(-22.5170124018609,27.346877819463,9.8553901742278));
#60215=CARTESIAN_POINT('Ctrl Pts',(-22.6294597286488,27.3757015038207,9.86124362252752));
#60216=CARTESIAN_POINT('Ctrl Pts',(-22.7428804865309,27.3994913370541,9.86709707082725));
#60217=CARTESIAN_POINT('Ctrl Pts',(-22.8564302284443,27.423308224494,9.87295717576878));
#60218=CARTESIAN_POINT('Ctrl Pts',(-22.9709552061766,27.4420797498071,9.87881728071031));
#60219=CARTESIAN_POINT('Ctrl Pts',(-23.0859705896342,27.4557526633389,9.88467738565183));
#60220=CARTESIAN_POINT('Ctrl Pts',(-23.2010634287541,27.4694347847223,9.89054143700728));
#60221=CARTESIAN_POINT('Ctrl Pts',(-23.3166469199654,27.4780114268376,9.89640548836271));
#60222=CARTESIAN_POINT('Ctrl Pts',(-23.4322344591452,27.4814814406426,9.90226953971816));
#60223=CARTESIAN_POINT('Ctrl Pts',(-23.547992351284,27.4849565685553,9.90814223351471));
#60224=CARTESIAN_POINT('Ctrl Pts',(-23.6637538915088,27.4833100532698,9.91401492731127));
#60225=CARTESIAN_POINT('Ctrl Pts',(-23.779035737802,27.4765927162176,9.91988762110782));
#60226=CARTESIAN_POINT('Ctrl Pts',(-23.8105979788894,27.4747536216999,9.92149546643126));
#60227=CARTESIAN_POINT('Ctrl Pts',(-23.8421243145612,27.4725347292978,9.9231033117547));
#60228=CARTESIAN_POINT('Ctrl Pts',(-23.873604958918,27.4699377496433,9.92471115707814));
#60229=CARTESIAN_POINT('Ctrl Pts',(-23.9885810015351,27.4604528598152,9.93058345404684));
#60230=CARTESIAN_POINT('Ctrl Pts',(-24.1033319762176,27.4458889064202,9.93645575101554));
#60231=CARTESIAN_POINT('Ctrl Pts',(-24.2173730606687,27.4262606843973,9.94232804798424));
#60232=CARTESIAN_POINT('Ctrl Pts',(-24.3312663569315,27.4066578989912,9.94819273492245));
#60233=CARTESIAN_POINT('Ctrl Pts',(-24.4444511888035,27.382003965661,9.95405742186065));
#60234=CARTESIAN_POINT('Ctrl Pts',(-24.5564460792985,27.3523655685146,9.95992210879885));
#60235=CARTESIAN_POINT('Ctrl Pts',(-24.6683257900591,27.3227576526044,9.96578076427366));
#60236=CARTESIAN_POINT('Ctrl Pts',(-24.7790175963813,27.2881755742929,9.97163941974847));
#60237=CARTESIAN_POINT('Ctrl Pts',(-24.8880491315122,27.2487372562152,9.97749807522328));
#60238=CARTESIAN_POINT('Ctrl Pts',(-25.0013395344395,27.2077584426965,9.98358557494119));
#60239=CARTESIAN_POINT('Ctrl Pts',(-25.1128368706313,27.1615363544954,9.9896730746591));
#60240=CARTESIAN_POINT('Ctrl Pts',(-25.2220270074075,27.1102608325769,9.99576057437701));
#60241=CARTESIAN_POINT('Ctrl Pts',(-25.326990707516,27.06097003888,10.0016124444604));
#60242=CARTESIAN_POINT('Ctrl Pts',(-25.4298220881502,27.0070099371923,10.0074643145438));
#60243=CARTESIAN_POINT('Ctrl Pts',(-25.5300845543172,26.9485983296077,10.0133161846272));
#60244=CARTESIAN_POINT('Ctrl Pts',(-25.6303317546121,26.8901956157214,10.0191671637101));
#60245=CARTESIAN_POINT('Ctrl Pts',(-25.7280104610633,26.8273429516219,10.0250181427931));
#60246=CARTESIAN_POINT('Ctrl Pts',(-25.8227096632119,26.7603035570541,10.0308691218761));
#60247=CARTESIAN_POINT('Ctrl Pts',(-25.9174173797301,26.6932581349997,10.0367206270184));
#60248=CARTESIAN_POINT('Ctrl Pts',(-26.0091447219964,26.6220254730379,10.0425721321607));
#60249=CARTESIAN_POINT('Ctrl Pts',(-26.0975111860478,26.5469110620944,10.0484236373029));
#60250=CARTESIAN_POINT('Ctrl Pts',(-26.185906994679,26.4717717072897,10.0542770856028));
#60251=CARTESIAN_POINT('Ctrl Pts',(-26.2709393910506,26.3927483079109,10.0601305339026));
#60252=CARTESIAN_POINT('Ctrl Pts',(-26.3522629047852,26.3101849346872,10.0659839822024));
#60253=CARTESIAN_POINT('Ctrl Pts',(-26.4336789010134,26.2275276689804,10.0718440871439));
#60254=CARTESIAN_POINT('Ctrl Pts',(-26.5113773057353,26.1413226888989,10.0777041920854));
#60255=CARTESIAN_POINT('Ctrl Pts',(-26.585051247904,26.0519491064392,10.083564297027));
#60256=CARTESIAN_POINT('Ctrl Pts',(-26.6587748048618,25.9625153364655,10.0894283483824));
#60257=CARTESIAN_POINT('Ctrl Pts',(-26.7284682547061,25.8699090446739,10.0952923997379));
#60258=CARTESIAN_POINT('Ctrl Pts',(-26.7938676005712,25.7745389981715,10.1011564510933));
#60259=CARTESIAN_POINT('Ctrl Pts',(-26.8593633320171,25.6790283952582,10.1070291448899));
#60260=CARTESIAN_POINT('Ctrl Pts',(-26.9205521110534,25.5807462578784,10.1129018386864));
#60261=CARTESIAN_POINT('Ctrl Pts',(-26.977215427752,25.4801267009194,10.118774532483));
#60262=CARTESIAN_POINT('Ctrl Pts',(-26.9927288960029,25.4525787493833,10.1203823778064));
#60263=CARTESIAN_POINT('Ctrl Pts',(-27.0079034255219,25.4248557088185,10.1219902231297));
#60264=CARTESIAN_POINT('Ctrl Pts',(-27.0227351657991,25.3969667369354,10.1235980684531));
#60265=CARTESIAN_POINT('Ctrl Pts',(-27.0799881477026,25.289310671451,10.1298046185599));
#60266=CARTESIAN_POINT('Ctrl Pts',(-27.1323036867167,25.1788532239254,10.1360111686667));
#60267=CARTESIAN_POINT('Ctrl Pts',(-27.1794144389584,25.0660601879827,10.1422177187735));
#60268=CARTESIAN_POINT('Ctrl Pts',(-27.2264356367954,24.9534815640945,10.1484124706417));
#60269=CARTESIAN_POINT('Ctrl Pts',(-27.2682716265022,24.8385765123253,10.1546072225098));
#60270=CARTESIAN_POINT('Ctrl Pts',(-27.304701012513,24.7218350532766,10.1608019743779));
#60271=CARTESIAN_POINT('Ctrl Pts',(-27.3410394327568,24.6053851027469,10.1669812576803));
#60272=CARTESIAN_POINT('Ctrl Pts',(-27.3719980621105,24.4871082138234,10.1731605409826));
#60273=CARTESIAN_POINT('Ctrl Pts',(-27.3974039812322,24.3675130313621,10.1793398242849));
#60274=CARTESIAN_POINT('Ctrl Pts',(-27.4227708432076,24.2481017055262,10.1855096080225));
#60275=CARTESIAN_POINT('Ctrl Pts',(-27.4426019248462,24.127376457047,10.1916793917601));
#60276=CARTESIAN_POINT('Ctrl Pts',(-27.4567739781773,24.0058611226663,10.1978491754977));
#60277=CARTESIAN_POINT('Ctrl Pts',(-27.4709185023618,23.8845818312486,10.2040069744595));
#60278=CARTESIAN_POINT('Ctrl Pts',(-27.4794258697771,23.7625158535628,10.2101647734214));
#60279=CARTESIAN_POINT('Ctrl Pts',(-27.4822239293042,23.640196560829,10.2163225723832));
#60280=CARTESIAN_POINT('Ctrl Pts',(-27.4829076246993,23.6103082984926,10.2178272075611));
#60281=CARTESIAN_POINT('Ctrl Pts',(-27.4832506848561,23.5804049575549,10.219331842739));
#60282=CARTESIAN_POINT('Ctrl Pts',(-27.4832525242572,23.5504943982643,10.220836477917));
#60283=CARTESIAN_POINT('',(-27.4832508647148,23.5466314190111,11.4708364779651));
#60284=CARTESIAN_POINT('Ctrl Pts',(-27.4832525242573,23.5504943973073,10.2208364779651));
#60285=CARTESIAN_POINT('Ctrl Pts',(-27.4832599837499,23.429194869929,10.2269383878019));
#60286=CARTESIAN_POINT('Ctrl Pts',(-27.477651540728,23.3079927501158,10.2330402976386));
#60287=CARTESIAN_POINT('Ctrl Pts',(-27.4664800506225,23.187415074988,10.2391422074754));
#60288=CARTESIAN_POINT('Ctrl Pts',(-27.4552948215406,23.0666891104377,10.2452516215926));
#60289=CARTESIAN_POINT('Ctrl Pts',(-27.4385329343121,22.9465894793983,10.2513610357098));
#60290=CARTESIAN_POINT('Ctrl Pts',(-27.4162986599985,22.8276348362125,10.257470449827));
#60291=CARTESIAN_POINT('Ctrl Pts',(-27.3940139545882,22.7084103837659,10.2635937211292));
#60292=CARTESIAN_POINT('Ctrl Pts',(-27.3662321195515,22.5903364639223,10.2697169924315));
#60293=CARTESIAN_POINT('Ctrl Pts',(-27.3331081374179,22.473919652774,10.2758402637338));
#60294=CARTESIAN_POINT('Ctrl Pts',(-27.2999435623553,22.35736017462,10.2819710390105));
#60295=CARTESIAN_POINT('Ctrl Pts',(-27.2614238943629,22.2424621963302,10.2881018142873));
#60296=CARTESIAN_POINT('Ctrl Pts',(-27.2177527405278,22.1297134726727,10.2942325895641));
#60297=CARTESIAN_POINT('Ctrl Pts',(-27.1739841470157,22.0167131825178,10.3003770439106));
#60298=CARTESIAN_POINT('Ctrl Pts',(-27.1250412370664,21.9058720615225,10.3065214982572));
#60299=CARTESIAN_POINT('Ctrl Pts',(-27.0711746862601,21.7976555496452,10.3126659526038));
#60300=CARTESIAN_POINT('Ctrl Pts',(-27.0424812173744,21.7400111103785,10.3159389616785));
#60301=CARTESIAN_POINT('Ctrl Pts',(-27.0123914487368,21.6831109281034,10.3192119707533));
#60302=CARTESIAN_POINT('Ctrl Pts',(-26.9809482499123,21.6270219451551,10.322484979828));
#60303=CARTESIAN_POINT('Ctrl Pts',(-26.9245341682743,21.5263894210691,10.3283572767967));
#60304=CARTESIAN_POINT('Ctrl Pts',(-26.8635940462272,21.4280726043284,10.3342295737654));
#60305=CARTESIAN_POINT('Ctrl Pts',(-26.7983428459281,21.3325063084802,10.3401018707341));
#60306=CARTESIAN_POINT('Ctrl Pts',(-26.7331762060025,21.2370638589619,10.3459665576723));
#60307=CARTESIAN_POINT('Ctrl Pts',(-26.6637098289418,21.1443651801547,10.3518312446105));
#60308=CARTESIAN_POINT('Ctrl Pts',(-26.5902044815023,21.0548204763463,10.3576959315487));
#60309=CARTESIAN_POINT('Ctrl Pts',(-26.516774729711,20.9653678636601,10.3635545870235));
#60310=CARTESIAN_POINT('Ctrl Pts',(-26.4393145304274,20.8790630917514,10.3694132424984));
#60311=CARTESIAN_POINT('Ctrl Pts',(-26.3581274671624,20.7962867826753,10.3752718979732));
#60312=CARTESIAN_POINT('Ctrl Pts',(-26.2737691656977,20.7102771580581,10.3813593976911));
#60313=CARTESIAN_POINT('Ctrl Pts',(-26.185387172064,20.6280776409253,10.387446897409));
#60314=CARTESIAN_POINT('Ctrl Pts',(-26.0933678410765,20.5500769496348,10.3935343971269));
#60315=CARTESIAN_POINT('Ctrl Pts',(-26.0049103141682,20.4750954411338,10.3993862672103));
#60316=CARTESIAN_POINT('Ctrl Pts',(-25.9130921406373,20.403994045741,10.4052381372937));
#60317=CARTESIAN_POINT('Ctrl Pts',(-25.818292880096,20.337079337168,10.4110900073771));
#60318=CARTESIAN_POINT('Ctrl Pts',(-25.7235080536041,20.2701748169679,10.4169409864601));
#60319=CARTESIAN_POINT('Ctrl Pts',(-25.6257433802275,20.2074559544305,10.4227919655431));
#60320=CARTESIAN_POINT('Ctrl Pts',(-25.5254090948665,20.1491871764037,10.428642944626));
#60321=CARTESIAN_POINT('Ctrl Pts',(-25.4250657884878,20.0909131594531,10.4344944497683));
#60322=CARTESIAN_POINT('Ctrl Pts',(-25.3221527683472,20.0370902299994,10.4403459549106));
#60323=CARTESIAN_POINT('Ctrl Pts',(-25.2171060371046,19.9879374990924,10.4461974600529));
#60324=CARTESIAN_POINT('Ctrl Pts',(-25.1120244221296,19.9387684456335,10.4520509083527));
#60325=CARTESIAN_POINT('Ctrl Pts',(-25.0048080613511,19.8942728496352,10.4579043566524));
#60326=CARTESIAN_POINT('Ctrl Pts',(-24.8959134861679,19.8546219230423,10.4637578049522));
#60327=CARTESIAN_POINT('Ctrl Pts',(-24.7868950742064,19.8149259047357,10.4696179098937));
#60328=CARTESIAN_POINT('Ctrl Pts',(-24.6761950272078,19.780085694034,10.4754780148353));
#60329=CARTESIAN_POINT('Ctrl Pts',(-24.5642857048657,19.7502228313224,10.4813381197768));
#60330=CARTESIAN_POINT('Ctrl Pts',(-24.4523010185992,19.7203398578419,10.4872021711323));
#60331=CARTESIAN_POINT('Ctrl Pts',(-24.3391058381589,19.6954409953037,10.4930662224877));
#60332=CARTESIAN_POINT('Ctrl Pts',(-24.225181675889,19.6755964630455,10.4989302738432));
#60333=CARTESIAN_POINT('Ctrl Pts',(-24.1110896121454,19.655722683908,10.5048029676397));
#60334=CARTESIAN_POINT('Ctrl Pts',(-23.9962668307793,19.6409181546278,10.5106756614363));
#60335=CARTESIAN_POINT('Ctrl Pts',(-23.8811989931845,19.6312011873473,10.5165483552328));
#60336=CARTESIAN_POINT('Ctrl Pts',(-23.8496953441007,19.6285408442509,10.5181562005562));
#60337=CARTESIAN_POINT('Ctrl Pts',(-23.8181733178316,19.6262615495909,10.5197640458795));
#60338=CARTESIAN_POINT('Ctrl Pts',(-23.7866428440123,19.6243629993408,10.5213718912029));
#60339=CARTESIAN_POINT('Ctrl Pts',(-23.6714848103734,19.6174289673683,10.5272441881716));
#60340=CARTESIAN_POINT('Ctrl Pts',(-23.555828503464,19.6155545071208,10.5331164851403));
#60341=CARTESIAN_POINT('Ctrl Pts',(-23.4401559353756,19.6187938024845,10.538988782109));
#60342=CARTESIAN_POINT('Ctrl Pts',(-23.3246332697492,19.6220288999786,10.5448534690472));
#60343=CARTESIAN_POINT('Ctrl Pts',(-23.2090947942574,19.6303645628526,10.5507181559854));
#60344=CARTESIAN_POINT('Ctrl Pts',(-23.0940265761364,19.6438031364664,10.5565828429236));
#60345=CARTESIAN_POINT('Ctrl Pts',(-22.9790766984739,19.6572278893487,10.5624414983984));
#60346=CARTESIAN_POINT('Ctrl Pts',(-22.8645965243403,19.6757450667168,10.5683001538732));
#60347=CARTESIAN_POINT('Ctrl Pts',(-22.7510703772143,19.6993050010258,10.5741588093481));
#60348=CARTESIAN_POINT('Ctrl Pts',(-22.6331097987892,19.7237852071202,10.580246309066));
#60349=CARTESIAN_POINT('Ctrl Pts',(-22.5161797515239,19.753710137564,10.5863338087839));
#60350=CARTESIAN_POINT('Ctrl Pts',(-22.4008161118513,19.7889648643203,10.5924213085018));
#60351=CARTESIAN_POINT('Ctrl Pts',(-22.2899178674166,19.822854981834,10.5982731785852));
#60352=CARTESIAN_POINT('Ctrl Pts',(-22.1804674552739,19.8616698333616,10.6041250486686));
#60353=CARTESIAN_POINT('Ctrl Pts',(-22.0729279690916,19.9052558051208,10.609976918752));
#60354=CARTESIAN_POINT('Ctrl Pts',(-21.9654048567738,19.9488351405195,10.615827897835));
#60355=CARTESIAN_POINT('Ctrl Pts',(-21.8597924749099,19.9971839965083,10.6216788769179));
#60356=CARTESIAN_POINT('Ctrl Pts',(-21.7565350395982,20.0501001695035,10.6275298560009));
#60357=CARTESIAN_POINT('Ctrl Pts',(-21.6532683204493,20.1030211001721,10.6333813611432));
#60358=CARTESIAN_POINT('Ctrl Pts',(-21.5523573366669,20.1605099756308,10.6392328662855));
#60359=CARTESIAN_POINT('Ctrl Pts',(-21.4542221079744,20.2223184183378,10.6450843714278));
#60360=CARTESIAN_POINT('Ctrl Pts',(-21.3560542907092,20.2841473862829,10.6509378197276));
#60361=CARTESIAN_POINT('Ctrl Pts',(-21.2606644110128,20.3502985535691,10.6567912680273));
#60362=CARTESIAN_POINT('Ctrl Pts',(-21.168443286942,20.4204803799852,10.6626447163271));
#60363=CARTESIAN_POINT('Ctrl Pts',(-21.0761172874275,20.4907420183779,10.6685048212686));
#60364=CARTESIAN_POINT('Ctrl Pts',(-20.9869675652956,20.5650432144048,10.6743649262102));
#60365=CARTESIAN_POINT('Ctrl Pts',(-20.9013517049511,20.6430522616612,10.6802250311517));
#60366=CARTESIAN_POINT('Ctrl Pts',(-20.815678187683,20.7211138431287,10.6860890825072));
#60367=CARTESIAN_POINT('Ctrl Pts',(-20.7335435631579,20.8028879569104,10.6919531338626));
#60368=CARTESIAN_POINT('Ctrl Pts',(-20.6552671859175,20.888007455121,10.6978171852181));
#60369=CARTESIAN_POINT('Ctrl Pts',(-20.5768754449228,20.9732524024802,10.7036898790146));
#60370=CARTESIAN_POINT('Ctrl Pts',(-20.5023535650337,21.0618522592839,10.7095625728112));
#60371=CARTESIAN_POINT('Ctrl Pts',(-20.4319794731352,21.1534083289424,10.7154352666078));
#60372=CARTESIAN_POINT('Ctrl Pts',(-20.4127122239881,21.1784748492689,10.7170431119311));
#60373=CARTESIAN_POINT('Ctrl Pts',(-20.3937556236361,21.2037628034635,10.7186509572544));
#60374=CARTESIAN_POINT('Ctrl Pts',(-20.3751147836853,21.2292636732183,10.7202588025778));
#60375=CARTESIAN_POINT('Ctrl Pts',(-20.3070332671685,21.3223999208331,10.7261310995465));
#60376=CARTESIAN_POINT('Ctrl Pts',(-20.2429391154088,21.4186902871183,10.7320033965152));
#60377=CARTESIAN_POINT('Ctrl Pts',(-20.1831384621879,21.5177585359016,10.7378756934839));
#60378=CARTESIAN_POINT('Ctrl Pts',(-20.1234153058645,21.6166984001021,10.7437403804221));
#60379=CARTESIAN_POINT('Ctrl Pts',(-20.0679747948712,21.7184086372237,10.7496050673603));
#60380=CARTESIAN_POINT('Ctrl Pts',(-20.0170816423457,21.8224815785119,10.7554697542985));
#60381=CARTESIAN_POINT('Ctrl Pts',(-19.9662408302416,21.9264474872952,10.7613284097733));
#60382=CARTESIAN_POINT('Ctrl Pts',(-19.919938254969,22.0327708979367,10.7671870652482));
#60383=CARTESIAN_POINT('Ctrl Pts',(-19.878393927761,22.1410174935541,10.773045720723));
#60384=CARTESIAN_POINT('Ctrl Pts',(-19.8352268425406,22.2534922965384,10.7791332204409));
#60385=CARTESIAN_POINT('Ctrl Pts',(-19.7971975410473,22.3680432006966,10.7852207201588));
#60386=CARTESIAN_POINT('Ctrl Pts',(-19.7644989963251,22.4841572407186,10.7913082198767));
#60387=CARTESIAN_POINT('Ctrl Pts',(-19.7330661183788,22.5957768396601,10.7971600899601));
#60388=CARTESIAN_POINT('Ctrl Pts',(-19.7065591165186,22.708840380511,10.8030119600435));
#60389=CARTESIAN_POINT('Ctrl Pts',(-19.6850990746519,22.8228752200368,10.808863830127));
#60390=CARTESIAN_POINT('Ctrl Pts',(-19.6636423002717,22.9368926967214,10.8147148092099));
#60391=CARTESIAN_POINT('Ctrl Pts',(-19.6472310344,23.0518807718897,10.8205657882929));
#60392=CARTESIAN_POINT('Ctrl Pts',(-19.6359352774022,23.167356419476,10.8264167673759));
#60393=CARTESIAN_POINT('Ctrl Pts',(-19.6246385048072,23.2828424494341,10.8322682725182));
#60394=CARTESIAN_POINT('Ctrl Pts',(-19.6184581956386,23.3988157275114,10.8381197776605));
#60395=CARTESIAN_POINT('Ctrl Pts',(-19.6174124241694,23.5147886254762,10.8439712828028));
#60396=CARTESIAN_POINT('Ctrl Pts',(-19.6163663054223,23.6308000355159,10.8498247311025));
#60397=CARTESIAN_POINT('Ctrl Pts',(-19.6204581185209,23.746810652045,10.8556781794023));
#60398=CARTESIAN_POINT('Ctrl Pts',(-19.6296538395216,23.8623340834315,10.8615316277021));
#60399=CARTESIAN_POINT('Ctrl Pts',(-19.638860018054,23.9779888900451,10.8673917326436));
#60400=CARTESIAN_POINT('Ctrl Pts',(-19.6531816567781,24.0931549933546,10.8732518375851));
#60401=CARTESIAN_POINT('Ctrl Pts',(-19.6725329750599,24.207352250227,10.8791119425267));
#60402=CARTESIAN_POINT('Ctrl Pts',(-19.6918973252433,24.321626411804,10.8849759938821));
#60403=CARTESIAN_POINT('Ctrl Pts',(-19.7162980127044,24.4349300246412,10.8908400452375));
#60404=CARTESIAN_POINT('Ctrl Pts',(-19.7455987744352,24.5467959514079,10.896704096593));
#60405=CARTESIAN_POINT('Ctrl Pts',(-19.7749427196399,24.6588267462206,10.9025767903895));
#60406=CARTESIAN_POINT('Ctrl Pts',(-19.8092010304325,24.7694152327351,10.9084494841861));
#60407=CARTESIAN_POINT('Ctrl Pts',(-19.848188507946,24.8781120739913,10.9143221779827));
#60408=CARTESIAN_POINT('Ctrl Pts',(-19.8588626271084,24.9078714508511,10.915930023306));
#60409=CARTESIAN_POINT('Ctrl Pts',(-19.8698909611422,24.9374891680603,10.9175378686294));
#60410=CARTESIAN_POINT('Ctrl Pts',(-19.8812691064921,24.9669563206325,10.9191457139527));
#60411=CARTESIAN_POINT('Ctrl Pts',(-19.9228252484156,25.0745785329279,10.9250180109214));
#60412=CARTESIAN_POINT('Ctrl Pts',(-19.9691903429848,25.1805510432062,10.9308903078901));
#60413=CARTESIAN_POINT('Ctrl Pts',(-20.020213334682,25.2844129243793,10.9367626048588));
#60414=CARTESIAN_POINT('Ctrl Pts',(-20.0711702046341,25.3881402088028,10.942627291797));
#60415=CARTESIAN_POINT('Ctrl Pts',(-20.1267727871619,25.489761935863,10.9484919787352));
#60416=CARTESIAN_POINT('Ctrl Pts',(-20.1868211923751,25.5888350357117,10.9543566656733));
#60417=CARTESIAN_POINT('Ctrl Pts',(-20.2468078415624,25.6878062450789,10.9602153211481));
#60418=CARTESIAN_POINT('Ctrl Pts',(-20.3112310060147,25.7842336893521,10.9660739766229));
#60419=CARTESIAN_POINT('Ctrl Pts',(-20.3798442130501,25.8776975027025,10.9719326320977));
#60420=CARTESIAN_POINT('Ctrl Pts',(-20.4511375123865,25.974812094925,10.9780201318156));
#60421=CARTESIAN_POINT('Ctrl Pts',(-20.5269546603845,26.0687264041915,10.9841076315335));
#60422=CARTESIAN_POINT('Ctrl Pts',(-20.606968400833,26.1590007995461,10.9901951312514));
#60423=CARTESIAN_POINT('Ctrl Pts',(-20.683885039139,26.2457809322692,10.9960470013348));
#60424=CARTESIAN_POINT('Ctrl Pts',(-20.7646791348476,26.3291973546086,11.0018988714182));
#60425=CARTESIAN_POINT('Ctrl Pts',(-20.8490184962602,26.4088927129365,11.0077507415016));
#60426=CARTESIAN_POINT('Ctrl Pts',(-20.9333450162381,26.4885759369214,11.0136017205845));
#60427=CARTESIAN_POINT('Ctrl Pts',(-21.0212154282485,26.5645389395703,11.0194526996675));
#60428=CARTESIAN_POINT('Ctrl Pts',(-21.112261192523,26.636461732336,11.0253036787504));
#60429=CARTESIAN_POINT('Ctrl Pts',(-21.203315142688,26.7083909916531,11.0311551838927));
#60430=CARTESIAN_POINT('Ctrl Pts',(-21.2975446882551,26.7762790627085,11.037006689035));
#60431=CARTESIAN_POINT('Ctrl Pts',(-21.3945493493224,26.8398471555821,11.0428581941773));
#60432=CARTESIAN_POINT('Ctrl Pts',(-21.4915862235257,26.9034363580353,11.0487116424771));
#60433=CARTESIAN_POINT('Ctrl Pts',(-21.5913997001102,26.9627025032952,11.0545650907769));
#60434=CARTESIAN_POINT('Ctrl Pts',(-21.6935621782513,27.0174113009795,11.0604185390766));
#60435=CARTESIAN_POINT('Ctrl Pts',(-21.7958408373142,27.0721823144466,11.0662786440181));
#60436=CARTESIAN_POINT('Ctrl Pts',(-21.9004734651811,27.1223854405725,11.0721387489597));
#60437=CARTESIAN_POINT('Ctrl Pts',(-22.007009741309,27.1678333103257,11.0779988539012));
#60438=CARTESIAN_POINT('Ctrl Pts',(-22.1136177629511,27.2133117863747,11.0838629052566));
#60439=CARTESIAN_POINT('Ctrl Pts',(-22.2221315994582,27.2540284846328,11.0897269566121));
#60440=CARTESIAN_POINT('Ctrl Pts',(-22.3320845844241,27.2898455379241,11.0955910079675));
#60441=CARTESIAN_POINT('Ctrl Pts',(-22.4421996181414,27.3257153784023,11.1014637017641));
#60442=CARTESIAN_POINT('Ctrl Pts',(-22.5537576366229,27.3566710518781,11.1073363955606));
#60443=CARTESIAN_POINT('Ctrl Pts',(-22.6662804973064,27.3826254835897,11.1132090893572));
#60444=CARTESIAN_POINT('Ctrl Pts',(-22.6970873742863,27.3897313728283,11.1148169346806));
#60445=CARTESIAN_POINT('Ctrl Pts',(-22.7279665387796,27.3964626821058,11.1164247800041));
#60446=CARTESIAN_POINT('Ctrl Pts',(-22.7589081185634,27.4028183026846,11.1180326253275));
#60447=CARTESIAN_POINT('Ctrl Pts',(-22.871915347879,27.4260307914202,11.1239049222962));
#60448=CARTESIAN_POINT('Ctrl Pts',(-22.9861340979795,27.4443056937332,11.1297772192649));
#60449=CARTESIAN_POINT('Ctrl Pts',(-23.1010949312611,27.4575209445337,11.1356495162336));
#60450=CARTESIAN_POINT('Ctrl Pts',(-23.2159067844326,27.4707190694187,11.1415142031718));
#60451=CARTESIAN_POINT('Ctrl Pts',(-23.3314584014597,27.4788705353511,11.14737889011));
#60452=CARTESIAN_POINT('Ctrl Pts',(-23.4472689712856,27.4819040150133,11.1532435770482));
#60453=CARTESIAN_POINT('Ctrl Pts',(-23.5629604371909,27.4849343749316,11.159102232523));
#60454=CARTESIAN_POINT('Ctrl Pts',(-23.6789099154205,27.4828572072494,11.1649608879978));
#60455=CARTESIAN_POINT('Ctrl Pts',(-23.7946309368751,27.4756529182893,11.1708195434726));
#60456=CARTESIAN_POINT('Ctrl Pts',(-23.9148721233533,27.468167223457,11.1769070431906));
#60457=CARTESIAN_POINT('Ctrl Pts',(-24.0348661900667,27.4551456502361,11.1829945429085));
#60458=CARTESIAN_POINT('Ctrl Pts',(-24.1540663722603,27.4366258855989,11.1890820426264));
#60459=CARTESIAN_POINT('Ctrl Pts',(-24.2686526576711,27.4188229678734,11.1949339127098));
#60460=CARTESIAN_POINT('Ctrl Pts',(-24.3825049272021,27.395939652118,11.2007857827932));
#60461=CARTESIAN_POINT('Ctrl Pts',(-24.4951429695548,27.3680622519971,11.2066376528766));
#60462=CARTESIAN_POINT('Ctrl Pts',(-24.6077638617413,27.3401890964639,11.2124886319595));
#60463=CARTESIAN_POINT('Ctrl Pts',(-24.7191704931788,27.30732346776,11.2183396110425));
#60464=CARTESIAN_POINT('Ctrl Pts',(-24.8288944407653,27.2696024572009,11.2241905901254));
#60465=CARTESIAN_POINT('Ctrl Pts',(-24.9386282535905,27.2318780551601,11.2300420952677));
#60466=CARTESIAN_POINT('Ctrl Pts',(-25.046678690865,27.189297537853,11.23589360041));
#60467=CARTESIAN_POINT('Ctrl Pts',(-25.1525947255868,27.1420471379699,11.2417451055523));
#60468=CARTESIAN_POINT('Ctrl Pts',(-25.2585459327178,27.0947810472577,11.247598553852));
#60469=CARTESIAN_POINT('Ctrl Pts',(-25.3623609505943,27.0428421586952,11.2534520021518));
#60470=CARTESIAN_POINT('Ctrl Pts',(-25.4636115304138,26.9864635761469,11.2593054504515));
#60471=CARTESIAN_POINT('Ctrl Pts',(-25.5649772541291,26.9300208789076,11.2651655553931));
#60472=CARTESIAN_POINT('Ctrl Pts',(-25.6637723575134,26.8691286114636,11.2710256603346));
#60473=CARTESIAN_POINT('Ctrl Pts',(-25.7595957865131,26.8040643551386,11.2768857652761));
#60474=CARTESIAN_POINT('Ctrl Pts',(-25.8554837465946,26.7389562821092,11.2827498166316));
#60475=CARTESIAN_POINT('Ctrl Pts',(-25.9483957168541,26.6696708722956,11.288613867987));
#60476=CARTESIAN_POINT('Ctrl Pts',(-26.0379634543475,26.596526216922,11.2944779193424));
#60477=CARTESIAN_POINT('Ctrl Pts',(-26.1276631968066,26.5232737609274,11.300350613139));
#60478=CARTESIAN_POINT('Ctrl Pts',(-26.2140085625529,26.4461509820488,11.3062233069355));
#60479=CARTESIAN_POINT('Ctrl Pts',(-26.2966678378037,26.365513082046,11.3120960007321));
#60480=CARTESIAN_POINT('Ctrl Pts',(-26.3192985646483,26.343435773931,11.3137038460556));
#60481=CARTESIAN_POINT('Ctrl Pts',(-26.3416532255523,26.3210951727694,11.315311691379));
#60482=CARTESIAN_POINT('Ctrl Pts',(-26.3637255513613,26.2984989849086,11.3169195367024));
#60483=CARTESIAN_POINT('Ctrl Pts',(-26.443276563939,26.2170599177125,11.3227143824589));
#60484=CARTESIAN_POINT('Ctrl Pts',(-26.5194391806909,26.1320095390702,11.3285092282153));
#60485=CARTESIAN_POINT('Ctrl Pts',(-26.5918609065626,26.0436653522937,11.3343040739718));
#60486=CARTESIAN_POINT('Ctrl Pts',(-26.664166907015,25.9554623340401,11.3400896599246));
#60487=CARTESIAN_POINT('Ctrl Pts',(-26.7327436429163,25.8639763052162,11.3458752458775));
#60488=CARTESIAN_POINT('Ctrl Pts',(-26.797274995011,25.7695619113698,11.3516608318304));
#60489=CARTESIAN_POINT('Ctrl Pts',(-26.8617474105324,25.6752337463202,11.3574411337996));
#60490=CARTESIAN_POINT('Ctrl Pts',(-26.9221815439285,25.5779828781755,11.3632214357688));
#60491=CARTESIAN_POINT('Ctrl Pts',(-26.9783013276128,25.4781971504011,11.369001737738));
#60492=CARTESIAN_POINT('Ctrl Pts',(-27.0343843040768,25.3784768689814,11.3747782485869));
#60493=CARTESIAN_POINT('Ctrl Pts',(-27.0861583463047,25.2762254011407,11.3805547594359));
#60494=CARTESIAN_POINT('Ctrl Pts',(-27.1333910325968,25.1718589831335,11.3863312702848));
#60495=CARTESIAN_POINT('Ctrl Pts',(-27.1806048955167,25.0675341576774,11.392105479054));
#60496=CARTESIAN_POINT('Ctrl Pts',(-27.2232808258136,24.9610964447608,11.3978796878231));
#60497=CARTESIAN_POINT('Ctrl Pts',(-27.2612330492045,24.8529852743008,11.4036538965923));
#60498=CARTESIAN_POINT('Ctrl Pts',(-27.299192984464,24.7448521357169,11.4094292786771));
#60499=CARTESIAN_POINT('Ctrl Pts',(-27.3324271438471,24.6350452581093,11.415204660762));
#60500=CARTESIAN_POINT('Ctrl Pts',(-27.3607986331734,24.5240222213549,11.4209800428468));
#60501=CARTESIAN_POINT('Ctrl Pts',(-27.3891719891915,24.41299187988,11.4267558049208));
#60502=CARTESIAN_POINT('Ctrl Pts',(-27.4126819414435,24.3007456345179,11.4325315669949));
#60503=CARTESIAN_POINT('Ctrl Pts',(-27.4312423860383,24.1877529242258,11.4383073290689));
#60504=CARTESIAN_POINT('Ctrl Pts',(-27.4498198554455,24.074656569881,11.4440883890368));
#60505=CARTESIAN_POINT('Ctrl Pts',(-27.4634386876286,23.9608128045669,11.4498694490047));
#60506=CARTESIAN_POINT('Ctrl Pts',(-27.4720645078,23.8466978454926,11.4556505089726));
#60507=CARTESIAN_POINT('Ctrl Pts',(-27.4796174155358,23.7467769405775,11.4607124986368));
#60508=CARTESIAN_POINT('Ctrl Pts',(-27.4833429503497,23.6466483696507,11.4657744883009));
#60509=CARTESIAN_POINT('Ctrl Pts',(-27.4832508647148,23.5466314190111,11.4708364779651));
#60510=CARTESIAN_POINT('',(-27.4846964008749,23.5516548132277,12.7208364779651));
#60511=CARTESIAN_POINT('Ctrl Pts',(-27.4835131464095,23.5466311775283,11.4708364779651));
#60512=CARTESIAN_POINT('Ctrl Pts',(-27.4862622880016,23.2504300277655,11.4858264680025));
#60513=CARTESIAN_POINT('Ctrl Pts',(-27.3202535819363,21.6472835327814,11.567112095165));
#60514=CARTESIAN_POINT('Ctrl Pts',(-25.1236967614753,19.1724649525787,11.714693359452));
#60515=CARTESIAN_POINT('Ctrl Pts',(-20.7176596990131,19.8601077274406,11.9135802708271));
#60516=CARTESIAN_POINT('Ctrl Pts',(-18.9145352855183,23.9386807047295,12.1124671822019));
#60517=CARTESIAN_POINT('Ctrl Pts',(-21.3712419772517,27.660321124278,12.311354093577));
#60518=CARTESIAN_POINT('Ctrl Pts',(-25.8302746188912,27.6051569835897,12.5102410049518));
#60519=CARTESIAN_POINT('Ctrl Pts',(-27.4525860600378,25.010103460541,12.6467351330812));
#60520=CARTESIAN_POINT('Ctrl Pts',(-27.4895040349668,23.6284897608082,12.7169336240856));
#60521=CARTESIAN_POINT('Ctrl Pts',(-27.4891511394909,23.5516564009483,12.7208364779651));
#60522=CARTESIAN_POINT('',(-27.482741765581,23.5531935453585,13.9708364359043));
#60523=CARTESIAN_POINT('Ctrl Pts',(-27.4832522818912,23.5516542985269,12.7208364779651));
#60524=CARTESIAN_POINT('Ctrl Pts',(-27.4832930552431,23.4372546857449,12.7266562861414));
#60525=CARTESIAN_POINT('Ctrl Pts',(-27.4783382662288,23.3226513759092,12.7324760943177));
#60526=CARTESIAN_POINT('Ctrl Pts',(-27.4683607881123,23.208321703911,12.7382959024941));
#60527=CARTESIAN_POINT('Ctrl Pts',(-27.4583958193384,23.0941353736489,12.7441084140396));
#60528=CARTESIAN_POINT('Ctrl Pts',(-27.4434207162572,22.9802224150746,12.7499209255851));
#60529=CARTESIAN_POINT('Ctrl Pts',(-27.423460347452,22.8670613315512,12.7557334371306));
#60530=CARTESIAN_POINT('Ctrl Pts',(-27.4035194302777,22.7540105249298,12.7615402843103));
#60531=CARTESIAN_POINT('Ctrl Pts',(-27.3786029801996,22.6417105489896,12.7673471314901));
#60532=CARTESIAN_POINT('Ctrl Pts',(-27.3487877011582,22.5306351689815,12.7731539786698));
#60533=CARTESIAN_POINT('Ctrl Pts',(-27.3189918880954,22.4196323085352,12.7789570346403));
#60534=CARTESIAN_POINT('Ctrl Pts',(-27.2843037141321,22.3098528600586,12.7847600906107));
#60535=CARTESIAN_POINT('Ctrl Pts',(-27.2448508933787,22.2017600601401,12.7905631465812));
#60536=CARTESIAN_POINT('Ctrl Pts',(-27.2054112340786,22.0937033199585,12.7963642666533));
#60537=CARTESIAN_POINT('Ctrl Pts',(-27.1612102309948,21.9873325055485,12.8021653867254));
#60538=CARTESIAN_POINT('Ctrl Pts',(-27.11242513171,21.8830946604364,12.8079665067975));
#60539=CARTESIAN_POINT('Ctrl Pts',(-27.063643982512,21.7788652553715,12.813767157158));
#60540=CARTESIAN_POINT('Ctrl Pts',(-27.0102796537688,21.6767688577968,12.8195678075185));
#60541=CARTESIAN_POINT('Ctrl Pts',(-26.9525567705978,21.5772307715662,12.825368457879));
#60542=CARTESIAN_POINT('Ctrl Pts',(-26.8948239780363,21.4776755974545,12.8311701040475));
#60543=CARTESIAN_POINT('Ctrl Pts',(-26.8327313557761,21.380679971763,12.836971750216));
#60544=CARTESIAN_POINT('Ctrl Pts',(-26.7665481149689,21.2866422028151,12.8427733963845));
#60545=CARTESIAN_POINT('Ctrl Pts',(-26.7002959762773,21.1925065389433,12.8485810821658));
#60546=CARTESIAN_POINT('Ctrl Pts',(-26.6299449589489,21.1013352252773,12.8543887679471));
#60547=CARTESIAN_POINT('Ctrl Pts',(-26.5558060586206,21.0134953504133,12.8601964537284));
#60548=CARTESIAN_POINT('Ctrl Pts',(-26.4816264793564,20.925607279088,12.8660073261023));
#60549=CARTESIAN_POINT('Ctrl Pts',(-26.4036551647765,20.8410545951663,12.8718181984763));
#60550=CARTESIAN_POINT('Ctrl Pts',(-26.322240325152,20.7601678245713,12.8776290708503));
#60551=CARTESIAN_POINT('Ctrl Pts',(-26.2406953369027,20.6791517495154,12.8834492324036));
#60552=CARTESIAN_POINT('Ctrl Pts',(-26.1556961415334,20.6018135745485,12.8892693939569));
#60553=CARTESIAN_POINT('Ctrl Pts',(-26.0676246149804,20.5284440013119,12.8950895555102));
#60554=CARTESIAN_POINT('Ctrl Pts',(-26.0024289188029,20.4741315510499,12.899397979574));
#60555=CARTESIAN_POINT('Ctrl Pts',(-25.9355503310069,20.4219929789331,12.9037064036378));
#60556=CARTESIAN_POINT('Ctrl Pts',(-25.8671533126791,20.3721304806912,12.9080148277016));
#60557=CARTESIAN_POINT('Ctrl Pts',(-25.7739295265685,20.304168879664,12.9138871246703));
#60558=CARTESIAN_POINT('Ctrl Pts',(-25.6775567558279,20.2401986991976,12.919759421639));
#60559=CARTESIAN_POINT('Ctrl Pts',(-25.5784116302886,20.1805255886336,12.9256317186077));
#60560=CARTESIAN_POINT('Ctrl Pts',(-25.479394988958,20.1209298096817,12.9314964055459));
#60561=CARTESIAN_POINT('Ctrl Pts',(-25.3776134884321,20.0656202377682,12.9373610924841));
#60562=CARTESIAN_POINT('Ctrl Pts',(-25.273475137793,20.0148610611736,12.9432257794223));
#60563=CARTESIAN_POINT('Ctrl Pts',(-25.1694438869288,19.9641540872148,12.9490844348971));
#60564=CARTESIAN_POINT('Ctrl Pts',(-25.0630609765168,19.917988380251,12.9549430903719));
#60565=CARTESIAN_POINT('Ctrl Pts',(-24.954761006217,19.8765833924012,12.9608017458467));
#60566=CARTESIAN_POINT('Ctrl Pts',(-24.8422307436875,19.8335610892568,12.9668892455646));
#60567=CARTESIAN_POINT('Ctrl Pts',(-24.7276309936318,19.795679237366,12.9729767452825));
#60568=CARTESIAN_POINT('Ctrl Pts',(-24.6114749692762,19.7631301494662,12.9790642450005));
#60569=CARTESIAN_POINT('Ctrl Pts',(-24.4998150110944,19.7318409432979,12.9849161150839));
#60570=CARTESIAN_POINT('Ctrl Pts',(-24.3867174514184,19.7054794673777,12.9907679851673));
#60571=CARTESIAN_POINT('Ctrl Pts',(-24.2726550889171,19.6841661972576,12.9966198552507));
#60572=CARTESIAN_POINT('Ctrl Pts',(-24.158610093448,19.6628561722766,13.0024708343336));
#60573=CARTESIAN_POINT('Ctrl Pts',(-24.043600993476,19.6465929007108,13.0083218134166));
#60574=CARTESIAN_POINT('Ctrl Pts',(-23.9281109047522,19.6354457612507,13.0141727924996));
#60575=CARTESIAN_POINT('Ctrl Pts',(-23.8126104323579,19.6242976195555,13.0200242976419));
#60576=CARTESIAN_POINT('Ctrl Pts',(-23.6966292967386,19.6182665641003,13.0258758027842));
#60577=CARTESIAN_POINT('Ctrl Pts',(-23.5806551489824,19.6173700416035,13.0317273079265));
#60578=CARTESIAN_POINT('Ctrl Pts',(-23.4646424887362,19.6164732213911,13.0375807562262));
#60579=CARTESIAN_POINT('Ctrl Pts',(-23.3486372341189,19.6207143277486,13.043434204526));
#60580=CARTESIAN_POINT('Ctrl Pts',(-23.2331257325736,19.6300587108124,13.0492876528258));
#60581=CARTESIAN_POINT('Ctrl Pts',(-23.1174828693683,19.6394137204689,13.0551477577673));
#60582=CARTESIAN_POINT('Ctrl Pts',(-23.0023352922621,19.6538835571578,13.0610078627089));
#60583=CARTESIAN_POINT('Ctrl Pts',(-22.8881630335975,19.6733818224095,13.0668679676504));
#60584=CARTESIAN_POINT('Ctrl Pts',(-22.7739138870627,19.6928932185223,13.0727320190059));
#60585=CARTESIAN_POINT('Ctrl Pts',(-22.6606417698388,19.7174396987215,13.0785960703613));
#60586=CARTESIAN_POINT('Ctrl Pts',(-22.5488136435096,19.7468843989424,13.0844601217167));
#60587=CARTESIAN_POINT('Ctrl Pts',(-22.436820704845,19.7763724947739,13.0903328155133));
#60588=CARTESIAN_POINT('Ctrl Pts',(-22.3262763976908,19.810773095985,13.0962055093099));
#60589=CARTESIAN_POINT('Ctrl Pts',(-22.2176298202984,19.8499004256005,13.1020782031064));
#60590=CARTESIAN_POINT('Ctrl Pts',(-22.1878842048435,19.860612833929,13.1036860484298));
#60591=CARTESIAN_POINT('Ctrl Pts',(-22.1582807047688,19.8716792745307,13.1052938937531));
#60592=CARTESIAN_POINT('Ctrl Pts',(-22.1288282193865,19.8830953323938,13.1069017390765));
#60593=CARTESIAN_POINT('Ctrl Pts',(-22.0212595757361,19.9247899413284,13.1127740360452));
#60594=CARTESIAN_POINT('Ctrl Pts',(-21.9153468214851,19.9712913758882,13.1186463330139));
#60595=CARTESIAN_POINT('Ctrl Pts',(-21.8115506889431,20.0224479875033,13.1245186299826));
#60596=CARTESIAN_POINT('Ctrl Pts',(-21.7078890679457,20.0735383042125,13.1303833169208));
#60597=CARTESIAN_POINT('Ctrl Pts',(-21.606338981239,20.1292716199616,13.136248003859));
#60598=CARTESIAN_POINT('Ctrl Pts',(-21.5073432410617,20.1894474748295,13.1421126907972));
#60599=CARTESIAN_POINT('Ctrl Pts',(-21.4084493118058,20.2495614425978,13.147971346272));
#60600=CARTESIAN_POINT('Ctrl Pts',(-21.3121048549879,20.3141086483293,13.1538300017469));
#60601=CARTESIAN_POINT('Ctrl Pts',(-21.2187294188977,20.3828420792116,13.1596886572217));
#60602=CARTESIAN_POINT('Ctrl Pts',(-21.1217066560299,20.4542602984438,13.1657761569396));
#60603=CARTESIAN_POINT('Ctrl Pts',(-21.0278899953097,20.530198244076,13.1718636566575));
#60604=CARTESIAN_POINT('Ctrl Pts',(-20.9377186461754,20.6103280943972,13.1779511563754));
#60605=CARTESIAN_POINT('Ctrl Pts',(-20.8510375710491,20.6873563482964,13.1838030264588));
#60606=CARTESIAN_POINT('Ctrl Pts',(-20.7677251935074,20.7682577275535,13.1896548965422));
#60607=CARTESIAN_POINT('Ctrl Pts',(-20.6881384393773,20.8526995808587,13.1955067666256));
#60608=CARTESIAN_POINT('Ctrl Pts',(-20.6085638030542,20.937128577124,13.2013577457086));
#60609=CARTESIAN_POINT('Ctrl Pts',(-20.5327139457,21.0250966748513,13.2072087247916));
#60610=CARTESIAN_POINT('Ctrl Pts',(-20.4609083813151,21.1162349227772,13.2130597038745));
#60611=CARTESIAN_POINT('Ctrl Pts',(-20.3890963609188,21.2073813649086,13.2189112090168));
#60612=CARTESIAN_POINT('Ctrl Pts',(-20.3213296121823,21.3016981991171,13.2247627141591));
#60613=CARTESIAN_POINT('Ctrl Pts',(-20.2578864094083,21.3987845870517,13.2306142193014));
#60614=CARTESIAN_POINT('Ctrl Pts',(-20.1944221385279,21.4959032152621,13.2364676676012));
#60615=CARTESIAN_POINT('Ctrl Pts',(-20.1352844945324,21.5957928801159,13.242321115901));
#60616=CARTESIAN_POINT('Ctrl Pts',(-20.0807072173211,21.6980256796289,13.2481745642008));
#60617=CARTESIAN_POINT('Ctrl Pts',(-20.0260678738943,21.8003747400344,13.2540346691423));
#60618=CARTESIAN_POINT('Ctrl Pts',(-19.9759994434011,21.9050718887787,13.2598947740839));
#60619=CARTESIAN_POINT('Ctrl Pts',(-19.9306887151902,22.0116665645623,13.2657548790254));
#60620=CARTESIAN_POINT('Ctrl Pts',(-19.8853474730397,22.1183330251887,13.2716189303809));
#60621=CARTESIAN_POINT('Ctrl Pts',(-19.8447704573727,22.226899171064,13.2774829817363));
#60622=CARTESIAN_POINT('Ctrl Pts',(-19.8090949346873,22.3368981587441,13.2833470330918));
#60623=CARTESIAN_POINT('Ctrl Pts',(-19.7733668334029,22.447059262974,13.2892197268884));
#60624=CARTESIAN_POINT('Ctrl Pts',(-19.7425547520611,22.5586570266223,13.2950924206849));
#60625=CARTESIAN_POINT('Ctrl Pts',(-19.7167451500187,22.6712131954641,13.3009651144815));
#60626=CARTESIAN_POINT('Ctrl Pts',(-19.7096789127216,22.7020291916575,13.3025729598048));
#60627=CARTESIAN_POINT('Ctrl Pts',(-19.7029873481038,22.7329169932492,13.3041808051281));
#60628=CARTESIAN_POINT('Ctrl Pts',(-19.696671552197,22.7638667265975,13.3057886504514));
#60629=CARTESIAN_POINT('Ctrl Pts',(-19.6736045142047,22.8769037350026,13.3116609474201));
#60630=CARTESIAN_POINT('Ctrl Pts',(-19.6554766176795,22.9911459088993,13.3175332443888));
#60631=CARTESIAN_POINT('Ctrl Pts',(-19.6424093234802,23.1061236539844,13.3234055413575));
#60632=CARTESIAN_POINT('Ctrl Pts',(-19.6293589634565,23.2209523970433,13.3292702282957));
#60633=CARTESIAN_POINT('Ctrl Pts',(-19.6213562102248,23.3365144086873,13.3351349152339));
#60634=CARTESIAN_POINT('Ctrl Pts',(-19.6184717722774,23.4523287864651,13.3409996021721));
#60635=CARTESIAN_POINT('Ctrl Pts',(-19.6155903007938,23.5680240564051,13.3468582576469));
#60636=CARTESIAN_POINT('Ctrl Pts',(-19.6178166847231,23.6839707654648,13.3527169131217));
#60637=CARTESIAN_POINT('Ctrl Pts',(-19.6251698916784,23.7996824197319,13.3585755685965));
#60638=CARTESIAN_POINT('Ctrl Pts',(-19.632810321374,23.9199138731327,13.3646630683144));
#60639=CARTESIAN_POINT('Ctrl Pts',(-19.64598630685,24.0398910827279,13.3707505680323));
#60640=CARTESIAN_POINT('Ctrl Pts',(-19.6646594575217,24.1590673327158,13.3768380677502));
#60641=CARTESIAN_POINT('Ctrl Pts',(-19.6826098241487,24.2736306122677,13.3826899378336));
#60642=CARTESIAN_POINT('Ctrl Pts',(-19.7056396399772,24.3874533384701,13.388541807917));
#60643=CARTESIAN_POINT('Ctrl Pts',(-19.7336619734197,24.5000554115013,13.3943936780003));
#60644=CARTESIAN_POINT('Ctrl Pts',(-19.7616800402071,24.6126403398431,13.4002446570833));
#60645=CARTESIAN_POINT('Ctrl Pts',(-19.7946890133718,24.7240045835165,13.4060956361663));
#60646=CARTESIAN_POINT('Ctrl Pts',(-19.8325511988876,24.8336798962333,13.4119466152492));
#60647=CARTESIAN_POINT('Ctrl Pts',(-19.8704167885783,24.9433650698164,13.4177981203915));
#60648=CARTESIAN_POINT('Ctrl Pts',(-19.9131363231405,25.0513606197998,13.4236496255338));
#60649=CARTESIAN_POINT('Ctrl Pts',(-19.9605229896014,25.157215759222,13.4295011306761));
#60650=CARTESIAN_POINT('Ctrl Pts',(-20.0079253921428,25.2631060508317,13.4353545789759));
#60651=CARTESIAN_POINT('Ctrl Pts',(-20.0599978395555,25.366854141428,13.4412080272757));
#60652=CARTESIAN_POINT('Ctrl Pts',(-20.1165066770451,25.4680320825499,13.4470614755754));
#60653=CARTESIAN_POINT('Ctrl Pts',(-20.1730797773534,25.5693250849607,13.452921580517));
#60654=CARTESIAN_POINT('Ctrl Pts',(-20.2340991359933,25.6680417429184,13.4587816854585));
#60655=CARTESIAN_POINT('Ctrl Pts',(-20.2992866557453,25.7637813599267,13.4646417904));
#60656=CARTESIAN_POINT('Ctrl Pts',(-20.364518075212,25.8595854515748,13.4705058417554));
#60657=CARTESIAN_POINT('Ctrl Pts',(-20.4339229981362,25.9524081799576,13.4763698931109));
#60658=CARTESIAN_POINT('Ctrl Pts',(-20.5071828596569,26.0418817117944,13.4822339444663));
#60659=CARTESIAN_POINT('Ctrl Pts',(-20.5805506915894,26.1314871097565,13.4881066382629));
#60660=CARTESIAN_POINT('Ctrl Pts',(-20.6577845263789,26.2177331529788,13.4939793320594));
#60661=CARTESIAN_POINT('Ctrl Pts',(-20.7385287356696,26.3002885850704,13.499852025856));
#60662=CARTESIAN_POINT('Ctrl Pts',(-20.760635149489,26.3228908813947,13.5014598711794));
#60663=CARTESIAN_POINT('Ctrl Pts',(-20.7830045008615,26.3452167731694,13.5030677165028));
#60664=CARTESIAN_POINT('Ctrl Pts',(-20.8056290753783,26.3672600011626,13.5046755618262));
#60665=CARTESIAN_POINT('Ctrl Pts',(-20.8882602951966,26.4477679822721,13.5105478587949));
#60666=CARTESIAN_POINT('Ctrl Pts',(-20.9745752563114,26.524772023834,13.5164201557637));
#60667=CARTESIAN_POINT('Ctrl Pts',(-21.0642445359001,26.5979161031613,13.5222924527324));
#60668=CARTESIAN_POINT('Ctrl Pts',(-21.1537976112236,26.6709653935707,13.5281571396706));
#60669=CARTESIAN_POINT('Ctrl Pts',(-21.2466960431651,26.7401644104516,13.5340218266087));
#60670=CARTESIAN_POINT('Ctrl Pts',(-21.3425734613611,26.8051937174014,13.5398865135469));
#60671=CARTESIAN_POINT('Ctrl Pts',(-21.4383522756347,26.8701561457801,13.5457451690218));
#60672=CARTESIAN_POINT('Ctrl Pts',(-21.5371036422464,26.9309571632024,13.5516038244966));
#60673=CARTESIAN_POINT('Ctrl Pts',(-21.6384285185044,26.9873178413138,13.5574624799714));
#60674=CARTESIAN_POINT('Ctrl Pts',(-21.7437112336749,27.0458800171542,13.5635499796893));
#60675=CARTESIAN_POINT('Ctrl Pts',(-21.8517722518342,27.0996476074844,13.5696374794072));
#60676=CARTESIAN_POINT('Ctrl Pts',(-21.9621308600668,27.1483573878799,13.5757249791251));
#60677=CARTESIAN_POINT('Ctrl Pts',(-22.0682178034569,27.1951817525409,13.5815768492085));
#60678=CARTESIAN_POINT('Ctrl Pts',(-22.1764273645156,27.2373323908848,13.5874287192919));
#60679=CARTESIAN_POINT('Ctrl Pts',(-22.2863086369991,27.2746229256082,13.5932805893753));
#60680=CARTESIAN_POINT('Ctrl Pts',(-22.3961731790597,27.3119077825085,13.5991315684583));
#60681=CARTESIAN_POINT('Ctrl Pts',(-22.5077085351043,27.3443338743233,13.6049825475412));
#60682=CARTESIAN_POINT('Ctrl Pts',(-22.6204463322158,27.3717639383776,13.6108335266242));
#60683=CARTESIAN_POINT('Ctrl Pts',(-22.7331942655399,27.3991964686586,13.6166850317665));
#60684=CARTESIAN_POINT('Ctrl Pts',(-22.8471444531569,27.4216319804948,13.6225365369087));
#60685=CARTESIAN_POINT('Ctrl Pts',(-22.9618166601015,27.4389839733115,13.628388042051));
#60686=CARTESIAN_POINT('Ctrl Pts',(-23.0765269471901,27.4563417283473,13.6342414903508));
#60687=CARTESIAN_POINT('Ctrl Pts',(-23.191959321854,27.4686125458157,13.6400949386506));
#60688=CARTESIAN_POINT('Ctrl Pts',(-23.3076274435509,27.4757616791302,13.6459483869503));
#60689=CARTESIAN_POINT('Ctrl Pts',(-23.423427105019,27.4829189425616,13.6518084918918));
#60690=CARTESIAN_POINT('Ctrl Pts',(-23.5394626357905,27.4849428708623,13.6576685968334));
#60691=CARTESIAN_POINT('Ctrl Pts',(-23.6552465998438,27.481850838446,13.6635287017749));
#60692=CARTESIAN_POINT('Ctrl Pts',(-23.7711085371503,27.4787567237393,13.6693927531303));
#60693=CARTESIAN_POINT('Ctrl Pts',(-23.8867181590657,27.4705398173159,13.6752568044858));
#60694=CARTESIAN_POINT('Ctrl Pts',(-24.0015938034672,27.4572693036564,13.6811208558412));
#60695=CARTESIAN_POINT('Ctrl Pts',(-24.1166387516373,27.4439792319089,13.6869935496378));
#60696=CARTESIAN_POINT('Ctrl Pts',(-24.2309471567365,27.425620753443,13.6928662434344));
#60697=CARTESIAN_POINT('Ctrl Pts',(-24.3440480950026,27.402314006239,13.6987389372309));
#60698=CARTESIAN_POINT('Ctrl Pts',(-24.3750132399536,27.3959330087285,13.7003467825543));
#60699=CARTESIAN_POINT('Ctrl Pts',(-24.4058879700136,27.3891813890663,13.7019546278777));
#60700=CARTESIAN_POINT('Ctrl Pts',(-24.4366628492207,27.3820622541338,13.7035624732011));
#60701=CARTESIAN_POINT('Ctrl Pts',(-24.5490612418088,27.3560611992589,13.7094347701699));
#60702=CARTESIAN_POINT('Ctrl Pts',(-24.6605029296012,27.3250669231564,13.7153070671386));
#60703=CARTESIAN_POINT('Ctrl Pts',(-24.770510317737,27.2891641294191,13.7211793641073));
#60704=CARTESIAN_POINT('Ctrl Pts',(-24.8803751450342,27.2533078628513,13.7270440510455));
#60705=CARTESIAN_POINT('Ctrl Pts',(-24.9888089796828,27.2125558555647,13.7329087379836));
#60706=CARTESIAN_POINT('Ctrl Pts',(-25.0953450357647,27.1670436721757,13.7387734249218));
#60707=CARTESIAN_POINT('Ctrl Pts',(-25.2017715261828,27.1215782952179,13.7446320803967));
#60708=CARTESIAN_POINT('Ctrl Pts',(-25.3063037422964,27.0713626410672,13.7504907358715));
#60709=CARTESIAN_POINT('Ctrl Pts',(-25.4084913175092,27.0165816584351,13.7563493913464));
#60710=CARTESIAN_POINT('Ctrl Pts',(-25.5146704294149,26.9596608823714,13.7624368910643));
#60711=CARTESIAN_POINT('Ctrl Pts',(-25.6183175666323,26.8978109966629,13.7685243907822));
#60712=CARTESIAN_POINT('Ctrl Pts',(-25.7189514283267,26.8312941491908,13.7746118905001));
#60713=CARTESIAN_POINT('Ctrl Pts',(-25.815690042194,26.7673519778886,13.7804637605835));
#60714=CARTESIAN_POINT('Ctrl Pts',(-25.9096439365277,26.6990976655203,13.7863156306669));
#60715=CARTESIAN_POINT('Ctrl Pts',(-26.0004125750353,26.6268098222407,13.7921675007503));
#60716=CARTESIAN_POINT('Ctrl Pts',(-26.0911673931926,26.5545329854423,13.7980184798333));
#60717=CARTESIAN_POINT('Ctrl Pts',(-26.178737596551,26.4782240962994,13.8038694589162));
#60718=CARTESIAN_POINT('Ctrl Pts',(-26.2627545283017,26.3982030085109,13.8097204379992));
#60719=CARTESIAN_POINT('Ctrl Pts',(-26.3467790139833,26.3181747260564,13.8155719431415));
#60720=CARTESIAN_POINT('Ctrl Pts',(-26.4272492936185,26.2344338665853,13.8214234482839));
#60721=CARTESIAN_POINT('Ctrl Pts',(-26.5038330054651,26.1473377026039,13.8272749534262));
#60722=CARTESIAN_POINT('Ctrl Pts',(-26.5804421490952,26.0602126158826,13.833128401726));
#60723=CARTESIAN_POINT('Ctrl Pts',(-26.6531618857459,25.9697303193629,13.8389818500258));
#60724=CARTESIAN_POINT('Ctrl Pts',(-26.7217000948503,25.8762811975002,13.8448352983256));
#60725=CARTESIAN_POINT('Ctrl Pts',(-26.790316246781,25.7827258036941,13.8506954032671));
#60726=CARTESIAN_POINT('Ctrl Pts',(-26.8547411350955,25.6861971838299,13.8565555082086));
#60727=CARTESIAN_POINT('Ctrl Pts',(-26.9147258973461,25.5871148176181,13.8624156131502));
#60728=CARTESIAN_POINT('Ctrl Pts',(-26.9747510555795,25.4879657256342,13.8682796645056));
#60729=CARTESIAN_POINT('Ctrl Pts',(-27.0303299360249,25.3862598247289,13.874143715861));
#60730=CARTESIAN_POINT('Ctrl Pts',(-27.0812603859501,25.2824397424722,13.8800077672165));
#60731=CARTESIAN_POINT('Ctrl Pts',(-27.1322658971921,25.1784666501384,13.8858804610131));
#60732=CARTESIAN_POINT('Ctrl Pts',(-27.1786091400688,25.0723735351517,13.8917531548096));
#60733=CARTESIAN_POINT('Ctrl Pts',(-27.2201366344214,24.9646215332459,13.8976258486062));
#60734=CARTESIAN_POINT('Ctrl Pts',(-27.2315061677044,24.9351208375963,13.8992336939295));
#60735=CARTESIAN_POINT('Ctrl Pts',(-27.2425150172714,24.9054958725268,13.9008415392527));
#60736=CARTESIAN_POINT('Ctrl Pts',(-27.2531606964563,24.8757562560714,13.902449384576));
#60737=CARTESIAN_POINT('Ctrl Pts',(-27.2983956243064,24.7493886113882,13.9092813363875));
#60738=CARTESIAN_POINT('Ctrl Pts',(-27.3371941851859,24.6206022531953,13.9161132881989));
#60739=CARTESIAN_POINT('Ctrl Pts',(-27.3693286506375,24.490011329321,13.9229452400104));
#60740=CARTESIAN_POINT('Ctrl Pts',(-27.4013201927057,24.3600012303152,13.9297468055792));
#60741=CARTESIAN_POINT('Ctrl Pts',(-27.4267066893909,24.2282026987485,13.9365483711479));
#60742=CARTESIAN_POINT('Ctrl Pts',(-27.4453101639974,24.0952433949541,13.9433499367166));
#60743=CARTESIAN_POINT('Ctrl Pts',(-27.4637638403299,23.9633547016042,13.9500967349473));
#60744=CARTESIAN_POINT('Ctrl Pts',(-27.4755432042108,23.8303239872224,13.956843533178));
#60745=CARTESIAN_POINT('Ctrl Pts',(-27.4805219515887,23.6967833715941,13.9635903314086));
#60746=CARTESIAN_POINT('Ctrl Pts',(-27.4823043522775,23.6489755863823,13.966005697544));
#60747=CARTESIAN_POINT('Ctrl Pts',(-27.4832156005693,23.601102622559,13.9684210636793));
#60748=CARTESIAN_POINT('Ctrl Pts',(-27.483251431705,23.5531940472059,13.9708364298146));
#60749=CARTESIAN_POINT('',(-27.4784560775625,23.547708951101,15.2208364779651));
#60750=CARTESIAN_POINT('Ctrl Pts',(-27.4792215614382,23.5531900791572,13.9708364779651));
#60751=CARTESIAN_POINT('Ctrl Pts',(-27.4732738423167,22.6912517315234,14.0143364172937));
#60752=CARTESIAN_POINT('Ctrl Pts',(-26.7690121054188,20.5068472925696,14.1241319937473));
#60753=CARTESIAN_POINT('Ctrl Pts',(-23.1558588724936,18.9150390011558,14.3002232073257));
#60754=CARTESIAN_POINT('Ctrl Pts',(-19.4373831253637,21.3765331205073,14.4991101187006));
#60755=CARTESIAN_POINT('Ctrl Pts',(-19.498285648829,25.8354910777289,14.6979970300756));
#60756=CARTESIAN_POINT('Ctrl Pts',(-23.282602187513,28.1945085674187,14.8968839414505));
#60757=CARTESIAN_POINT('Ctrl Pts',(-26.8142260262799,26.5219956903167,15.0711637574136));
#60758=CARTESIAN_POINT('Ctrl Pts',(-27.4735806028515,24.3741591972422,15.1791479362519));
#60759=CARTESIAN_POINT('Ctrl Pts',(-27.4784560775625,23.547708951101,15.2208364779651));
#60760=CARTESIAN_POINT('',(-27.4851245771615,23.5482800713537,16.4708358638271));
#60761=CARTESIAN_POINT('Ctrl Pts',(-27.4784560775625,23.547708951101,15.2208364779651));
#60762=CARTESIAN_POINT('Ctrl Pts',(-27.4813338772278,23.0598880961595,15.2454435733768));
#60763=CARTESIAN_POINT('Ctrl Pts',(-27.1706132058826,21.2613315865969,15.3363463059134));
#60764=CARTESIAN_POINT('Ctrl Pts',(-24.4745249954599,18.9910342604509,15.4935446755753));
#60765=CARTESIAN_POINT('Ctrl Pts',(-20.2141141537653,20.308195845668,15.6924315869498));
#60766=CARTESIAN_POINT('Ctrl Pts',(-19.0193316234954,24.6045326442667,15.8913184983251));
#60767=CARTESIAN_POINT('Ctrl Pts',(-21.9880812491219,27.9320754076229,16.0902054096997));
#60768=CARTESIAN_POINT('Ctrl Pts',(-26.2657817837741,27.2531790242803,16.2833774930198));
#60769=CARTESIAN_POINT('Ctrl Pts',(-27.4811614233285,24.7414234327789,16.4102539392149));
#60770=CARTESIAN_POINT('Ctrl Pts',(-27.4885259363507,23.5483003261169,16.4708347482849));
#60771=CARTESIAN_POINT('',(-27.4832509670657,23.5537607171193,17.7208364779651));
#60772=CARTESIAN_POINT('Ctrl Pts',(-27.4832520314764,23.5482689205262,16.4708364779651));
#60773=CARTESIAN_POINT('Ctrl Pts',(-27.4831953477107,23.4358793426591,16.4765507294599));
#60774=CARTESIAN_POINT('Ctrl Pts',(-27.4783216466447,23.3236146971763,16.4822649809548));
#60775=CARTESIAN_POINT('Ctrl Pts',(-27.4686601516153,23.2117695570205,16.4879792324497));
#60776=CARTESIAN_POINT('Ctrl Pts',(-27.4587314377627,23.0968309901582,16.4938515294185));
#60777=CARTESIAN_POINT('Ctrl Pts',(-27.4437245671289,22.9821370985901,16.4997238263873));
#60778=CARTESIAN_POINT('Ctrl Pts',(-27.4236562063245,22.8681726438799,16.5055961233561));
#60779=CARTESIAN_POINT('Ctrl Pts',(-27.4036138525219,22.7543558780523,16.5114608102944));
#60780=CARTESIAN_POINT('Ctrl Pts',(-27.3785231236498,22.6412670725969,16.5173254972326));
#60781=CARTESIAN_POINT('Ctrl Pts',(-27.3484525621856,22.5293874434603,16.5231901841709));
#60782=CARTESIAN_POINT('Ctrl Pts',(-27.3184129264115,22.4176228755186,16.5290488396457));
#60783=CARTESIAN_POINT('Ctrl Pts',(-27.2834037515192,22.3070654072013,16.5349074951206));
#60784=CARTESIAN_POINT('Ctrl Pts',(-27.2435447829588,22.1981869464696,16.5407661505955));
#60785=CARTESIAN_POINT('Ctrl Pts',(-27.2021288879794,22.0850555971636,16.5468536503134));
#60786=CARTESIAN_POINT('Ctrl Pts',(-27.1554766799918,21.9737375442461,16.5529411500312));
#60787=CARTESIAN_POINT('Ctrl Pts',(-27.1037799834882,21.8647461836355,16.5590286497491));
#60788=CARTESIAN_POINT('Ctrl Pts',(-27.0540843176646,21.7599735656369,16.5648805198325));
#60789=CARTESIAN_POINT('Ctrl Pts',(-26.9997276110195,21.6573512782908,16.570732389916));
#60790=CARTESIAN_POINT('Ctrl Pts',(-26.9409293496113,21.5573150724549,16.5765842599994));
#60791=CARTESIAN_POINT('Ctrl Pts',(-26.8821400407731,21.4572940980409,16.5824352390823));
#60792=CARTESIAN_POINT('Ctrl Pts',(-26.8189107312199,21.3598587785107,16.5882862181653));
#60793=CARTESIAN_POINT('Ctrl Pts',(-26.7515062255472,21.2654191050321,16.5941371972483));
#60794=CARTESIAN_POINT('Ctrl Pts',(-26.6840956595608,21.170970940518,16.5999887023906));
#60795=CARTESIAN_POINT('Ctrl Pts',(-26.6125093913782,21.0795192939652,16.6058402075329));
#60796=CARTESIAN_POINT('Ctrl Pts',(-26.5370543786821,20.9914434870741,16.6116917126751));
#60797=CARTESIAN_POINT('Ctrl Pts',(-26.4615743090189,20.9033384321249,16.6175451609749));
#60798=CARTESIAN_POINT('Ctrl Pts',(-26.3822232090504,20.818611759726,16.6233986092747));
#60799=CARTESIAN_POINT('Ctrl Pts',(-26.299346480719,20.7376076093062,16.6292520575744));
#60800=CARTESIAN_POINT('Ctrl Pts',(-26.2163755035511,20.6565113395775,16.6351121625159));
#60801=CARTESIAN_POINT('Ctrl Pts',(-26.129871191171,20.5791463305167,16.6409722674575));
#60802=CARTESIAN_POINT('Ctrl Pts',(-26.0402138375049,20.5058179872236,16.646832372399));
#60803=CARTESIAN_POINT('Ctrl Pts',(-25.9504961052224,20.4324402618808,16.6526964237545));
#60804=CARTESIAN_POINT('Ctrl Pts',(-25.8576214340356,20.3631048619561,16.6585604751099));
#60805=CARTESIAN_POINT('Ctrl Pts',(-25.7619996072334,20.2980742041968,16.6644245264654));
#60806=CARTESIAN_POINT('Ctrl Pts',(-25.6662368529464,20.2329477042294,16.6702972202619));
#60807=CARTESIAN_POINT('Ctrl Pts',(-25.5677192129509,20.1721388247979,16.6761699140585));
#60808=CARTESIAN_POINT('Ctrl Pts',(-25.4668816425129,20.1158643981889,16.6820426078551));
#60809=CARTESIAN_POINT('Ctrl Pts',(-25.4392740025383,20.1004574015422,16.6836504531781));
#60810=CARTESIAN_POINT('Ctrl Pts',(-25.4114925834006,20.0853900170775,16.6852582985012));
#60811=CARTESIAN_POINT('Ctrl Pts',(-25.3835465576077,20.0706660599206,16.6868661438242));
#60812=CARTESIAN_POINT('Ctrl Pts',(-25.281479922094,20.0168900854908,16.6927384407929));
#60813=CARTESIAN_POINT('Ctrl Pts',(-25.1768741769919,19.9675187069325,16.6986107377616));
#60814=CARTESIAN_POINT('Ctrl Pts',(-25.0701461693482,19.9227999365224,16.7044830347303));
#60815=CARTESIAN_POINT('Ctrl Pts',(-24.9635564727262,19.8781391180872,16.7103477216685));
#60816=CARTESIAN_POINT('Ctrl Pts',(-24.8548503606384,19.8381190757424,16.7162124086067));
#60817=CARTESIAN_POINT('Ctrl Pts',(-24.7444697382494,19.8029422611711,16.7220770955449));
#60818=CARTESIAN_POINT('Ctrl Pts',(-24.6342026354205,19.7678016237515,16.7279357510197));
#60819=CARTESIAN_POINT('Ctrl Pts',(-24.5222648391915,19.7374944314917,16.7337944064945));
#60820=CARTESIAN_POINT('Ctrl Pts',(-24.4091181011403,19.7121750267941,16.7396530619694));
#60821=CARTESIAN_POINT('Ctrl Pts',(-24.2915517518424,19.685866623848,16.7457405616873));
#60822=CARTESIAN_POINT('Ctrl Pts',(-24.1726805100561,19.6649437824608,16.7518280614052));
#60823=CARTESIAN_POINT('Ctrl Pts',(-24.0530399936515,19.6495226297273,16.7579155611231));
#60824=CARTESIAN_POINT('Ctrl Pts',(-23.9380304181026,19.634698385536,16.7637674312065));
#60825=CARTESIAN_POINT('Ctrl Pts',(-23.8223104616508,19.6249578980686,16.7696193012899));
#60826=CARTESIAN_POINT('Ctrl Pts',(-23.706365370323,19.6203520518327,16.7754711713734));
#60827=CARTESIAN_POINT('Ctrl Pts',(-23.5904379326896,19.6157469068789,16.7813221504563));
#60828=CARTESIAN_POINT('Ctrl Pts',(-23.4742858412814,19.6162748651003,16.7871731295393));
#60829=CARTESIAN_POINT('Ctrl Pts',(-23.3583971666563,19.6219347595548,16.7930241086223));
#60830=CARTESIAN_POINT('Ctrl Pts',(-23.2424980725241,19.6275951628883,16.7988756137646));
#60831=CARTESIAN_POINT('Ctrl Pts',(-23.1268628551714,19.6383883995298,16.8047271189069));
#60832=CARTESIAN_POINT('Ctrl Pts',(-23.0119765679496,19.6542612602904,16.8105786240492));
#60833=CARTESIAN_POINT('Ctrl Pts',(-22.8970521294927,19.6701393920825,16.816432072349));
#60834=CARTESIAN_POINT('Ctrl Pts',(-22.7828775249739,19.6911004456078,16.8222855206488));
#60835=CARTESIAN_POINT('Ctrl Pts',(-22.6699289890613,19.7170398503672,16.8281389689486));
#60836=CARTESIAN_POINT('Ctrl Pts',(-22.5568520061372,19.7430087538624,16.8339990738902));
#60837=CARTESIAN_POINT('Ctrl Pts',(-22.445004277946,19.7739672161251,16.8398591788317));
#60838=CARTESIAN_POINT('Ctrl Pts',(-22.3348483119114,19.8097603738981,16.8457192837733));
#60839=CARTESIAN_POINT('Ctrl Pts',(-22.2246181627281,19.8455776361227,16.8515833351288));
#60840=CARTESIAN_POINT('Ctrl Pts',(-22.1160824304322,19.88623593227,16.8574473864842));
#60841=CARTESIAN_POINT('Ctrl Pts',(-22.0096833958758,19.9315323521606,16.8633114378397));
#60842=CARTESIAN_POINT('Ctrl Pts',(-21.9031275503816,19.9768955299321,16.8691841316363));
#60843=CARTESIAN_POINT('Ctrl Pts',(-21.7987150589729,20.0269102962088,16.8750568254329));
#60844=CARTESIAN_POINT('Ctrl Pts',(-21.696863458051,20.0813279228709,16.8809295192294));
#60845=CARTESIAN_POINT('Ctrl Pts',(-21.6689781934873,20.0962265587555,16.8825373645528));
#60846=CARTESIAN_POINT('Ctrl Pts',(-21.6412847153458,20.1114549727474,16.8841452098762));
#60847=CARTESIAN_POINT('Ctrl Pts',(-21.6137911914852,20.1270075100991,16.8857530551995));
#60848=CARTESIAN_POINT('Ctrl Pts',(-21.5133772185241,20.1838096891512,16.8916253521682));
#60849=CARTESIAN_POINT('Ctrl Pts',(-21.415296409598,20.2451289344945,16.8974976491369));
#60850=CARTESIAN_POINT('Ctrl Pts',(-21.3199827450967,20.310748606864,16.9033699461056));
#60851=CARTESIAN_POINT('Ctrl Pts',(-21.224792599535,20.3762832413495,16.9092346330438));
#60852=CARTESIAN_POINT('Ctrl Pts',(-21.1323628044818,20.4461069878894,16.915099319982));
#60853=CARTESIAN_POINT('Ctrl Pts',(-21.0431025544099,20.5199574979717,16.9209640069202));
#60854=CARTESIAN_POINT('Ctrl Pts',(-20.9539341029175,20.5937320574274,16.926822662395));
#60855=CARTESIAN_POINT('Ctrl Pts',(-20.8679290293262,20.6715248812851,16.9326813178698));
#60856=CARTESIAN_POINT('Ctrl Pts',(-20.7854667807917,20.7530309188064,16.9385399733446));
#60857=CARTESIAN_POINT('Ctrl Pts',(-20.6997834841974,20.8377206539431,16.9446274730625));
#60858=CARTESIAN_POINT('Ctrl Pts',(-20.6179258011946,20.926419341357,16.9507149727804));
#60859=CARTESIAN_POINT('Ctrl Pts',(-20.5402809556218,21.0187391283648,16.9568024724983));
#60860=CARTESIAN_POINT('Ctrl Pts',(-20.4656415190728,21.1074854815033,16.9626543425817));
#60861=CARTESIAN_POINT('Ctrl Pts',(-20.3948951413588,21.1995774760393,16.9685062126651));
#60862=CARTESIAN_POINT('Ctrl Pts',(-20.3283469285187,21.2946343715823,16.9743580827485));
#60863=CARTESIAN_POINT('Ctrl Pts',(-20.2618088482491,21.3896767938487,16.9802090618314));
#60864=CARTESIAN_POINT('Ctrl Pts',(-20.1994678989163,21.4876828809792,16.9860600409144));
#60865=CARTESIAN_POINT('Ctrl Pts',(-20.1415869215794,21.5882413802424,16.9919110199973));
#60866=CARTESIAN_POINT('Ctrl Pts',(-20.0837007401858,21.6888089206825,16.9977625251396));
#60867=CARTESIAN_POINT('Ctrl Pts',(-20.0302755341599,21.7919289711599,17.0036140302819));
#60868=CARTESIAN_POINT('Ctrl Pts',(-19.9815287296177,21.8971646863294,17.0094655354241));
#60869=CARTESIAN_POINT('Ctrl Pts',(-19.9327657373229,22.0024353479889,17.0153189837239));
#60870=CARTESIAN_POINT('Ctrl Pts',(-19.8886844093961,22.1098226964525,17.0211724320236));
#60871=CARTESIAN_POINT('Ctrl Pts',(-19.8494541939489,22.2188695427157,17.0270258803234));
#60872=CARTESIAN_POINT('Ctrl Pts',(-19.810179365228,22.3280403989222,17.0328859852649));
#60873=CARTESIAN_POINT('Ctrl Pts',(-19.7757668003091,22.4388741305334,17.0387460902064));
#60874=CARTESIAN_POINT('Ctrl Pts',(-19.7463362150053,22.5508979121381,17.0446061951479));
#60875=CARTESIAN_POINT('Ctrl Pts',(-19.7168858100443,22.6629971347484,17.0504702465033));
#60876=CARTESIAN_POINT('Ctrl Pts',(-19.6924241523058,22.7762876000631,17.0563342978588));
#60877=CARTESIAN_POINT('Ctrl Pts',(-19.6730196016011,22.8902875282269,17.0621983492142));
#60878=CARTESIAN_POINT('Ctrl Pts',(-19.6535864524622,23.0044554695282,17.0680710430107));
#60879=CARTESIAN_POINT('Ctrl Pts',(-19.6392253365247,23.1193345518576,17.0739437368073));
#60880=CARTESIAN_POINT('Ctrl Pts',(-19.6299526907736,23.2344390467421,17.0798164306038));
#60881=CARTESIAN_POINT('Ctrl Pts',(-19.6274139954791,23.2659527319807,17.0814242759273));
#60882=CARTESIAN_POINT('Ctrl Pts',(-19.6252564167311,23.2974833231318,17.0830321212507));
#60883=CARTESIAN_POINT('Ctrl Pts',(-19.6234796121694,23.3290208918079,17.0846399665742));
#60884=CARTESIAN_POINT('Ctrl Pts',(-19.616990229211,23.4442048378238,17.0905122635429));
#60885=CARTESIAN_POINT('Ctrl Pts',(-19.6155623039825,23.559867519613,17.0963845605116));
#60886=CARTESIAN_POINT('Ctrl Pts',(-19.619248159034,23.6755267194855,17.1022568574803));
#60887=CARTESIAN_POINT('Ctrl Pts',(-19.6229292375102,23.7910360342203,17.1081215444185));
#60888=CARTESIAN_POINT('Ctrl Pts',(-19.6317109043909,23.9065414666524,17.1139862313567));
#60889=CARTESIAN_POINT('Ctrl Pts',(-19.6455936284308,24.0215569441134,17.1198509182949));
#60890=CARTESIAN_POINT('Ctrl Pts',(-19.6594620749581,24.136454135356,17.1257095737697));
#60891=CARTESIAN_POINT('Ctrl Pts',(-19.6784210946069,24.25086196595,17.1315682292445));
#60892=CARTESIAN_POINT('Ctrl Pts',(-19.7024191503464,24.3642963077809,17.1374268847194));
#60893=CARTESIAN_POINT('Ctrl Pts',(-19.7273545912803,24.4821614949153,17.1435143844373));
#60894=CARTESIAN_POINT('Ctrl Pts',(-19.7577307373536,24.5989751378054,17.1496018841552));
#60895=CARTESIAN_POINT('Ctrl Pts',(-19.7934305924967,24.7142018077215,17.1556893838731));
#60896=CARTESIAN_POINT('Ctrl Pts',(-19.8277486087554,24.8249683841057,17.1615412539565));
#60897=CARTESIAN_POINT('Ctrl Pts',(-19.8669857325947,24.9342681257803,17.1673931240399));
#60898=CARTESIAN_POINT('Ctrl Pts',(-19.9109865634842,25.0416385355941,17.1732449941233));
#60899=CARTESIAN_POINT('Ctrl Pts',(-19.9549806948472,25.1489925972867,17.1790959732063));
#60900=CARTESIAN_POINT('Ctrl Pts',(-20.0037369343856,25.2544175287995,17.1849469522892));
#60901=CARTESIAN_POINT('Ctrl Pts',(-20.057051365012,25.3574698980036,17.1907979313722));
#60902=CARTESIAN_POINT('Ctrl Pts',(-20.1103705891188,25.4605315326075,17.1966494365145));
#60903=CARTESIAN_POINT('Ctrl Pts',(-20.1682486290471,25.5612198136707,17.2025009416568));
#60904=CARTESIAN_POINT('Ctrl Pts',(-20.2304354875114,25.6591156835259,17.2083524467991));
#60905=CARTESIAN_POINT('Ctrl Pts',(-20.2926429968777,25.7570440624683,17.2142058950989));
#60906=CARTESIAN_POINT('Ctrl Pts',(-20.3591619484272,25.8521778375781,17.2200593433987));
#60907=CARTESIAN_POINT('Ctrl Pts',(-20.4296992952674,25.9441273192774,17.2259127916984));
#60908=CARTESIAN_POINT('Ctrl Pts',(-20.500316858388,26.0361813675039,17.23177289664));
#60909=CARTESIAN_POINT('Ctrl Pts',(-20.5749616861977,26.1250435662641,17.2376330015815));
#60910=CARTESIAN_POINT('Ctrl Pts',(-20.6533006942169,26.2103576144564,17.2434931065231));
#60911=CARTESIAN_POINT('Ctrl Pts',(-20.731692458655,26.2957291163205,17.2493571578785));
#60912=CARTESIAN_POINT('Ctrl Pts',(-20.813783064929,26.3775474186261,17.255221209234));
#60913=CARTESIAN_POINT('Ctrl Pts',(-20.8992041349393,26.4554945866809,17.2610852605894));
#60914=CARTESIAN_POINT('Ctrl Pts',(-20.9847510985551,26.5335566333016,17.266957954386));
#60915=CARTESIAN_POINT('Ctrl Pts',(-21.0736380060136,26.6077358951632,17.2728306481826));
#60916=CARTESIAN_POINT('Ctrl Pts',(-21.1654650906881,26.6777559867234,17.2787033419791));
#60917=CARTESIAN_POINT('Ctrl Pts',(-21.1906058103928,26.6969263164998,17.2803111873025));
#60918=CARTESIAN_POINT('Ctrl Pts',(-21.2159667629754,26.7157851448936,17.2819190326258));
#60919=CARTESIAN_POINT('Ctrl Pts',(-21.2415394104567,26.7343273932239,17.2835268779492));
#60920=CARTESIAN_POINT('Ctrl Pts',(-21.3349378102311,26.802048825803,17.2893991749179));
#60921=CARTESIAN_POINT('Ctrl Pts',(-21.4314749109175,26.865770746052,17.2952714718866));
#60922=CARTESIAN_POINT('Ctrl Pts',(-21.5307732972389,26.9251884750276,17.3011437688554));
#60923=CARTESIAN_POINT('Ctrl Pts',(-21.6299430007376,26.9845292033452,17.3070084557936));
#60924=CARTESIAN_POINT('Ctrl Pts',(-21.7318665222518,27.0395766225099,17.3128731427318));
#60925=CARTESIAN_POINT('Ctrl Pts',(-21.836135174072,27.0900675952672,17.31873782967));
#60926=CARTESIAN_POINT('Ctrl Pts',(-21.9402965921111,27.1405066412198,17.3245964851448));
#60927=CARTESIAN_POINT('Ctrl Pts',(-22.0467979734028,27.1863983824184,17.3304551406196));
#60928=CARTESIAN_POINT('Ctrl Pts',(-22.1552041548916,27.2275244860621,17.3363137960944));
#60929=CARTESIAN_POINT('Ctrl Pts',(-22.2678447773122,27.2702570115374,17.3424012958123));
#60930=CARTESIAN_POINT('Ctrl Pts',(-22.3825416496926,27.3078437762513,17.3484887955303));
#60931=CARTESIAN_POINT('Ctrl Pts',(-22.4987810655237,27.3400937890333,17.3545762952482));
#60932=CARTESIAN_POINT('Ctrl Pts',(-22.6105211873366,27.3710954964228,17.3604281653316));
#60933=CARTESIAN_POINT('Ctrl Pts',(-22.7236862226805,27.3971657897267,17.366280035415));
#60934=CARTESIAN_POINT('Ctrl Pts',(-22.8378030643677,27.4181854107016,17.3721319054984));
#60935=CARTESIAN_POINT('Ctrl Pts',(-22.9519025307281,27.439201831248,17.3779828845813));
#60936=CARTESIAN_POINT('Ctrl Pts',(-23.0669531088498,27.4551690336427,17.3838338636643));
#60937=CARTESIAN_POINT('Ctrl Pts',(-23.1824715060122,27.4660188828889,17.3896848427473));
#60938=CARTESIAN_POINT('Ctrl Pts',(-23.2980002893902,27.4768697076408,17.3955363478896));
#60939=CARTESIAN_POINT('Ctrl Pts',(-23.4139965638272,27.4826022259509,17.4013878530319));
#60940=CARTESIAN_POINT('Ctrl Pts',(-23.5299726349456,27.4832002462955,17.4072393581742));
#60941=CARTESIAN_POINT('Ctrl Pts',(-23.6459872191925,27.4837984652297,17.413092806474));
#60942=CARTESIAN_POINT('Ctrl Pts',(-23.7619811736217,27.4792587936734,17.4189462547738));
#60943=CARTESIAN_POINT('Ctrl Pts',(-23.8774682415842,27.4696171331572,17.4247997030735));
#60944=CARTESIAN_POINT('Ctrl Pts',(-23.9930866434205,27.4599645079794,17.4306598080151));
#60945=CARTESIAN_POINT('Ctrl Pts',(-24.1081965960394,27.4451983474994,17.4365199129566));
#60946=CARTESIAN_POINT('Ctrl Pts',(-24.2223182910646,27.4254062854286,17.4423800178982));
#60947=CARTESIAN_POINT('Ctrl Pts',(-24.3365168399086,27.4056008946428,17.4482440692536));
#60948=CARTESIAN_POINT('Ctrl Pts',(-24.4497254031651,27.380762951168,17.4541081206091));
#60949=CARTESIAN_POINT('Ctrl Pts',(-24.5614773730632,27.351030520501,17.4599721719645));
#60950=CARTESIAN_POINT('Ctrl Pts',(-24.6733940430572,27.3212542701663,17.4658448657611));
#60951=CARTESIAN_POINT('Ctrl Pts',(-24.7838494423243,27.2865692592731,17.4717175595577));
#60952=CARTESIAN_POINT('Ctrl Pts',(-24.8923949522613,27.2471624200894,17.4775902533542));
#60953=CARTESIAN_POINT('Ctrl Pts',(-24.9221128971362,27.2363734867173,17.4791980986775));
#60954=CARTESIAN_POINT('Ctrl Pts',(-24.9516878158783,27.2252308880272,17.4808059440008));
#60955=CARTESIAN_POINT('Ctrl Pts',(-24.9811108205685,27.2137390619219,17.482413789324));
#60956=CARTESIAN_POINT('Ctrl Pts',(-25.0885717925615,27.1717677263545,17.4882860862928));
#60957=CARTESIAN_POINT('Ctrl Pts',(-25.1943645086282,27.1249938430823,17.4941583832615));
#60958=CARTESIAN_POINT('Ctrl Pts',(-25.2980286283046,27.073570246025,17.5000306802302));
#60959=CARTESIAN_POINT('Ctrl Pts',(-25.4015584075147,27.0222132898655,17.5058953671684));
#60960=CARTESIAN_POINT('Ctrl Pts',(-25.5029647090802,26.9662187848019,17.5117600541066));
#60961=CARTESIAN_POINT('Ctrl Pts',(-25.6018052381816,26.9057883298201,17.5176247410448));
#60962=CARTESIAN_POINT('Ctrl Pts',(-25.7005441159865,26.845420023778,17.5234833965196));
#60963=CARTESIAN_POINT('Ctrl Pts',(-25.7967221193422,26.7806250563976,17.5293420519944));
#60964=CARTESIAN_POINT('Ctrl Pts',(-25.8899203371206,26.711651519524,17.5352007074693));
#60965=CARTESIAN_POINT('Ctrl Pts',(-25.9867589593731,26.6399838155492,17.5412882071872));
#60966=CARTESIAN_POINT('Ctrl Pts',(-26.0803798570342,26.5638046521469,17.5473757069051));
#60967=CARTESIAN_POINT('Ctrl Pts',(-26.1703446658817,26.4834429803983,17.553463206623));
#60968=CARTESIAN_POINT('Ctrl Pts',(-26.2568271953025,26.4061918782135,17.5593150767064));
#60969=CARTESIAN_POINT('Ctrl Pts',(-26.3399310694826,26.3250763339968,17.5651669467898));
#60970=CARTESIAN_POINT('Ctrl Pts',(-26.4193002199693,26.2404299166269,17.5710188168732));
#60971=CARTESIAN_POINT('Ctrl Pts',(-26.4986572857812,26.1557963874436,17.5768697959561));
#60972=CARTESIAN_POINT('Ctrl Pts',(-26.5742804758724,26.0676333555151,17.5827207750391));
#60973=CARTESIAN_POINT('Ctrl Pts',(-26.6458512269233,25.9763105932616,17.5885717541221));
#60974=CARTESIAN_POINT('Ctrl Pts',(-26.7174284128734,25.884979620213,17.5944232592644));
#60975=CARTESIAN_POINT('Ctrl Pts',(-26.7849521804736,25.7904886774804,17.6002747644067));
#60976=CARTESIAN_POINT('Ctrl Pts',(-26.8481452880373,25.6932393183217,17.606126269549));
#60977=CARTESIAN_POINT('Ctrl Pts',(-26.9113593806564,25.5959576647677,17.6119797178487));
#60978=CARTESIAN_POINT('Ctrl Pts',(-26.9702397285101,25.4959161198048,17.6178331661485));
#60979=CARTESIAN_POINT('Ctrl Pts',(-27.0245536938258,25.3935431856094,17.6236866144483));
#60980=CARTESIAN_POINT('Ctrl Pts',(-27.078929425914,25.2910538311581,17.6295467193898));
#60981=CARTESIAN_POINT('Ctrl Pts',(-27.1287282165997,25.1862281609553,17.6354068243314));
#60982=CARTESIAN_POINT('Ctrl Pts',(-27.1737644368266,25.0795172155745,17.6412669292729));
#60983=CARTESIAN_POINT('Ctrl Pts',(-27.2188309861292,24.9727344070507,17.6471309806284));
#60984=CARTESIAN_POINT('Ctrl Pts',(-27.2591284352385,24.8640641819386,17.6529950319838));
#60985=CARTESIAN_POINT('Ctrl Pts',(-27.2945207196926,24.7539737354384,17.6588590833393));
#60986=CARTESIAN_POINT('Ctrl Pts',(-27.3299651653089,24.6437210375963,17.6647317771358));
#60987=CARTESIAN_POINT('Ctrl Pts',(-27.3604899095314,24.5320443381553,17.6706044709324));
#60988=CARTESIAN_POINT('Ctrl Pts',(-27.3860097242403,24.4194221122888,17.676477164729));
#60989=CARTESIAN_POINT('Ctrl Pts',(-27.3929966226132,24.3885880307863,17.6780850100523));
#60990=CARTESIAN_POINT('Ctrl Pts',(-27.3996086647322,24.3576831084718,17.6796928553756));
#60991=CARTESIAN_POINT('Ctrl Pts',(-27.4058447799821,24.3267172217752,17.6813007006989));
#60992=CARTESIAN_POINT('Ctrl Pts',(-27.4386430309124,24.1638551062664,17.6897570091953));
#60993=CARTESIAN_POINT('Ctrl Pts',(-27.4611308481835,23.9988525117614,17.6982133176916));
#60994=CARTESIAN_POINT('Ctrl Pts',(-27.4730914971859,23.8327829739827,17.7066696261879));
#60995=CARTESIAN_POINT('Ctrl Pts',(-27.4797707214065,23.7400442205251,17.7113919101136));
#60996=CARTESIAN_POINT('Ctrl Pts',(-27.4831678227789,23.6469731076509,17.7161141940394));
#60997=CARTESIAN_POINT('Ctrl Pts',(-27.4832509670657,23.5537607171193,17.7208364779651));
#60998=CARTESIAN_POINT('',(-27.4767571638619,23.5506058536415,18.9708364779651));
#60999=CARTESIAN_POINT('Ctrl Pts',(-27.4846078470131,23.5537486008167,17.720837152879));
#61000=CARTESIAN_POINT('Ctrl Pts',(-27.4748958087803,22.5049130723347,17.7739539726106));
#61001=CARTESIAN_POINT('Ctrl Pts',(-26.5032239293697,20.1311413592398,17.8933664294671));
#61002=CARTESIAN_POINT('Ctrl Pts',(-22.4901423490843,19.0206921520514,18.0790745234486));
#61003=CARTESIAN_POINT('Ctrl Pts',(-19.1664228912539,21.9937216082251,18.2779614348238));
#61004=CARTESIAN_POINT('Ctrl Pts',(-19.8710711855328,26.397071011008,18.4768483461984));
#61005=CARTESIAN_POINT('Ctrl Pts',(-23.9565751937948,28.1844356017042,18.6757352575734));
#61006=CARTESIAN_POINT('Ctrl Pts',(-27.0299249841624,26.1385950912699,18.8403979681622));
#61007=CARTESIAN_POINT('Ctrl Pts',(-27.4772652391045,24.187090675563,18.9387650416262));
#61008=CARTESIAN_POINT('Ctrl Pts',(-27.4767571638619,23.5506058536415,18.9708364779651));
#61009=CARTESIAN_POINT('',(-27.4833068676715,23.5466220118607,20.2208364779651));
#61010=CARTESIAN_POINT('Ctrl Pts',(-27.4767571638619,23.5506058536415,18.9708364779651));
#61011=CARTESIAN_POINT('Ctrl Pts',(-27.4762149845553,22.871397597657,19.0050606787511));
#61012=CARTESIAN_POINT('Ctrl Pts',(-26.9851084914367,20.8757618441067,19.105580516662));
#61013=CARTESIAN_POINT('Ctrl Pts',(-23.8059484060801,18.9053229895029,19.2723959916981));
#61014=CARTESIAN_POINT('Ctrl Pts',(-19.7806098338932,20.8243499723508,19.4712829030729));
#61015=CARTESIAN_POINT('Ctrl Pts',(-19.219253287995,25.2482502888139,19.670169814448));
#61016=CARTESIAN_POINT('Ctrl Pts',(-22.637717838874,28.1118346329506,19.8690567258227));
#61017=CARTESIAN_POINT('Ctrl Pts',(-26.566569641527,26.8860911980051,20.0526122803286));
#61018=CARTESIAN_POINT('Ctrl Pts',(-27.4739820892811,24.5538076996726,20.1698721977093));
#61019=CARTESIAN_POINT('Ctrl Pts',(-27.4833068676715,23.5466220118607,20.2208364779651));
#61020=CARTESIAN_POINT('',(-27.4892473091168,23.551540164831,21.4708364779651));
#61021=CARTESIAN_POINT('Ctrl Pts',(-27.4833068676715,23.5466220118607,20.2208364779651));
#61022=CARTESIAN_POINT('Ctrl Pts',(-27.4861119991187,23.2436348385735,20.2361678348342));
#61023=CARTESIAN_POINT('Ctrl Pts',(-27.3155179850287,21.6336002486415,20.3177948288287));
#61024=CARTESIAN_POINT('Ctrl Pts',(-25.1011405181817,19.1644233871128,20.465717459947));
#61025=CARTESIAN_POINT('Ctrl Pts',(-20.6987015893344,19.8747378663381,20.6646043713225));
#61026=CARTESIAN_POINT('Ctrl Pts',(-18.916596204868,23.9625386907771,20.8634912826971));
#61027=CARTESIAN_POINT('Ctrl Pts',(-21.3924281154842,27.6714834911175,21.0623781940721));
#61028=CARTESIAN_POINT('Ctrl Pts',(-25.8511177112576,27.5933664625134,21.2612651054469));
#61029=CARTESIAN_POINT('Ctrl Pts',(-27.456025305492,24.9965071357817,21.3974178667446));
#61030=CARTESIAN_POINT('Ctrl Pts',(-27.4895458388405,23.6216486653013,21.4672749909173));
#61031=CARTESIAN_POINT('Ctrl Pts',(-27.4892473091168,23.551540164831,21.4708364779651));
#61032=CARTESIAN_POINT('',(-27.4820795739567,23.5532667202166,22.7208360305048));
#61033=CARTESIAN_POINT('Ctrl Pts',(-27.4892473091168,23.551540164831,21.4708364779651));
#61034=CARTESIAN_POINT('Ctrl Pts',(-27.4839888290946,22.3166073597353,21.5335706280423));
#61035=CARTESIAN_POINT('Ctrl Pts',(-26.1920695173065,19.7671546223778,21.6626004152444));
#61036=CARTESIAN_POINT('Ctrl Pts',(-21.8466825212323,19.221442065576,21.8579258395718));
#61037=CARTESIAN_POINT('Ctrl Pts',(-18.9874998465852,22.643588996177,22.0568127509464));
#61038=CARTESIAN_POINT('Ctrl Pts',(-20.3211000319204,26.8988828435244,22.2556996623214));
#61039=CARTESIAN_POINT('Ctrl Pts',(-24.6220175775656,28.0770693513325,22.4545865736964));
#61040=CARTESIAN_POINT('Ctrl Pts',(-27.2070963238024,25.7527407920887,22.6096316859959));
#61041=CARTESIAN_POINT('Ctrl Pts',(-27.4825225817787,23.9981564321766,22.6983811611705));
#61042=CARTESIAN_POINT('Ctrl Pts',(-27.4793788461029,23.5532850883259,22.7208349992202));
#61043=CARTESIAN_POINT('',(-27.4815531016315,23.5477787515071,23.970837000806));
#61044=CARTESIAN_POINT('Ctrl Pts',(-27.4832513827808,23.5532587505456,22.7208364779651));
#61045=CARTESIAN_POINT('Ctrl Pts',(-27.4833401065471,23.4371825470975,22.7266894177816));
#61046=CARTESIAN_POINT('Ctrl Pts',(-27.4782858174004,23.3210503319215,22.7325423575982));
#61047=CARTESIAN_POINT('Ctrl Pts',(-27.4681003776954,23.2053507259815,22.7383952974147));
#61048=CARTESIAN_POINT('Ctrl Pts',(-27.4579162907114,23.089666486025,22.7442474599064));
#61049=CARTESIAN_POINT('Ctrl Pts',(-27.4426024440398,22.9744151518856,22.7500996223982));
#61050=CARTESIAN_POINT('Ctrl Pts',(-27.4222226876323,22.860081457594,22.7559517848899));
#61051=CARTESIAN_POINT('Ctrl Pts',(-27.4018407298981,22.7457354135073,22.761804579505));
#61052=CARTESIAN_POINT('Ctrl Pts',(-27.3763918465693,22.6323076125064,22.7676573741202));
#61053=CARTESIAN_POINT('Ctrl Pts',(-27.3459911178517,22.5202731214364,22.7735101687353));
#61054=CARTESIAN_POINT('Ctrl Pts',(-27.3155797841398,22.4081995482394,22.7793650050402));
#61055=CARTESIAN_POINT('Ctrl Pts',(-27.2802132775954,22.2975206494814,22.785219841345));
#61056=CARTESIAN_POINT('Ctrl Pts',(-27.2400564931379,22.1886961699838,22.7910746776498));
#61057=CARTESIAN_POINT('Ctrl Pts',(-27.1998511006222,22.07973996314,22.7969366009818));
#61058=CARTESIAN_POINT('Ctrl Pts',(-27.1548439971764,21.9726430441766,22.8027985243139));
#61059=CARTESIAN_POINT('Ctrl Pts',(-27.10524824809,21.8678451920742,22.8086604476459));
#61060=CARTESIAN_POINT('Ctrl Pts',(-27.0556185970657,21.7629757037863,22.8145263779859));
#61061=CARTESIAN_POINT('Ctrl Pts',(-27.0013942467496,21.6604087757148,22.8203923083259));
#61062=CARTESIAN_POINT('Ctrl Pts',(-26.9428333494117,21.5605579834644,22.8262582386659));
#61063=CARTESIAN_POINT('Ctrl Pts',(-26.8841781246888,21.460546355835,22.8321336175952));
#61064=CARTESIAN_POINT('Ctrl Pts',(-26.8211726303032,21.3632599443681,22.8380089965245));
#61065=CARTESIAN_POINT('Ctrl Pts',(-26.7541174424854,21.2690820791851,22.8438843754538));
#61066=CARTESIAN_POINT('Ctrl Pts',(-26.721872079453,21.2237940179436,22.8467097157846));
#61067=CARTESIAN_POINT('Ctrl Pts',(-26.6886908358786,21.1792242803724,22.8495350561154));
#61068=CARTESIAN_POINT('Ctrl Pts',(-26.6546102315833,21.1354125222651,22.8523603964462));
#61069=CARTESIAN_POINT('Ctrl Pts',(-26.5837757812643,21.0443524642875,22.8582326934149));
#61070=CARTESIAN_POINT('Ctrl Pts',(-26.508812673025,20.9562591766196,22.8641049903835));
#61071=CARTESIAN_POINT('Ctrl Pts',(-26.4299985006656,20.8715304195308,22.8699772873522));
#61072=CARTESIAN_POINT('Ctrl Pts',(-26.3512864652145,20.7869114641824,22.8758419742904));
#61073=CARTESIAN_POINT('Ctrl Pts',(-26.2687335692525,20.7056486684967,22.8817066612286));
#61074=CARTESIAN_POINT('Ctrl Pts',(-26.1826590139729,20.628108607782,22.8875713481667));
#61075=CARTESIAN_POINT('Ctrl Pts',(-26.0966729809851,20.5506482921657,22.8934300036415));
#61076=CARTESIAN_POINT('Ctrl Pts',(-26.0071727979275,20.4769033712574,22.8992886591163));
#61077=CARTESIAN_POINT('Ctrl Pts',(-25.9145155751801,20.4072047654,22.9051473145911));
#61078=CARTESIAN_POINT('Ctrl Pts',(-25.8182390797001,20.3347836706077,22.911234814309));
#61079=CARTESIAN_POINT('Ctrl Pts',(-25.7185541928124,20.2667317731929,22.9173223140269));
#61080=CARTESIAN_POINT('Ctrl Pts',(-25.6159010759208,20.2033756155626,22.9234098137448));
#61081=CARTESIAN_POINT('Ctrl Pts',(-25.5172213664276,20.1424717928744,22.9292616838282));
#61082=CARTESIAN_POINT('Ctrl Pts',(-25.4157993222026,20.0859071894331,22.9351135539116));
#61083=CARTESIAN_POINT('Ctrl Pts',(-25.3120560965544,20.033928144092,22.9409654239949));
#61084=CARTESIAN_POINT('Ctrl Pts',(-25.2083286667556,19.9819570130332,22.9468164030779));
#61085=CARTESIAN_POINT('Ctrl Pts',(-25.1022811277337,19.9345702369693,22.9526673821608));
#61086=CARTESIAN_POINT('Ctrl Pts',(-24.994358657412,19.8919678930057,22.9585183612438));
#61087=CARTESIAN_POINT('Ctrl Pts',(-24.8864264838219,19.8493617186815,22.9643698663861));
#61088=CARTESIAN_POINT('Ctrl Pts',(-24.7766194283531,19.8115409833825,22.9702213715283));
#61089=CARTESIAN_POINT('Ctrl Pts',(-24.6654013671529,19.778657103394,22.9760728766706));
#61090=CARTESIAN_POINT('Ctrl Pts',(-24.554146372856,19.7457623033849,22.9819263249703));
#61091=CARTESIAN_POINT('Ctrl Pts',(-24.4414798373255,19.7178077357211,22.98777977327));
#61092=CARTESIAN_POINT('Ctrl Pts',(-24.3278787683951,19.6948943854263,22.9936332215698));
#61093=CARTESIAN_POINT('Ctrl Pts',(-24.2141485103808,19.6719549776765,22.9994933265113));
#61094=CARTESIAN_POINT('Ctrl Pts',(-24.0994820031775,19.6540683118901,23.0053534314528));
#61095=CARTESIAN_POINT('Ctrl Pts',(-23.9843644735907,19.6412838925385,23.0112135363943));
#61096=CARTESIAN_POINT('Ctrl Pts',(-23.8691694195529,19.6284908636806,23.0170775877497));
#61097=CARTESIAN_POINT('Ctrl Pts',(-23.7535231497996,19.6208069504418,23.0229416391052));
#61098=CARTESIAN_POINT('Ctrl Pts',(-23.6379122628203,19.6182295445362,23.0288056904606));
#61099=CARTESIAN_POINT('Ctrl Pts',(-23.5221309884716,19.6156483400488,23.0346783842571));
#61100=CARTESIAN_POINT('Ctrl Pts',(-23.406385612704,19.6181886542474,23.0405510780537));
#61101=CARTESIAN_POINT('Ctrl Pts',(-23.2911590707109,19.6257959351097,23.0464237718502));
#61102=CARTESIAN_POINT('Ctrl Pts',(-23.2596119710132,19.6278786813558,23.0480316171738));
#61103=CARTESIAN_POINT('Ctrl Pts',(-23.2281037082547,19.6303409369221,23.0496394624973));
#61104=CARTESIAN_POINT('Ctrl Pts',(-23.1966440548342,19.6331809156661,23.0512473078209));
#61105=CARTESIAN_POINT('Ctrl Pts',(-23.0817446769464,19.6435533055507,23.0571196047896));
#61106=CARTESIAN_POINT('Ctrl Pts',(-22.9671095780651,19.6590028697379,23.0629919017583));
#61107=CARTESIAN_POINT('Ctrl Pts',(-22.8532234517959,19.6795110701941,23.068864198727));
#61108=CARTESIAN_POINT('Ctrl Pts',(-22.7394849129014,19.6999926936513,23.0747288856652));
#61109=CARTESIAN_POINT('Ctrl Pts',(-22.6264938195099,19.7255198440746,23.0805935726034));
#61110=CARTESIAN_POINT('Ctrl Pts',(-22.5147311193557,19.7560221216389,23.0864582595416));
#61111=CARTESIAN_POINT('Ctrl Pts',(-22.4030833601422,19.7864930295202,23.0923169150165));
#61112=CARTESIAN_POINT('Ctrl Pts',(-22.2926618777462,19.821928779163,23.0981755704913));
#61113=CARTESIAN_POINT('Ctrl Pts',(-22.1839381143039,19.862207804087,23.1040342259661));
#61114=CARTESIAN_POINT('Ctrl Pts',(-22.070967504899,19.9040601632018,23.110121725684));
#61115=CARTESIAN_POINT('Ctrl Pts',(-21.9598303945074,19.9511417956007,23.1162092254019));
#61116=CARTESIAN_POINT('Ctrl Pts',(-21.8510394346335,20.0032588961237,23.1222967251198));
#61117=CARTESIAN_POINT('Ctrl Pts',(-21.7464594604354,20.0533586933339,23.1281485952032));
#61118=CARTESIAN_POINT('Ctrl Pts',(-21.6440477960159,20.1081111947209,23.1340004652866));
#61119=CARTESIAN_POINT('Ctrl Pts',(-21.5442393416026,20.1672952335335,23.13985233537));
#61120=CARTESIAN_POINT('Ctrl Pts',(-21.4444460839341,20.226470261038,23.145703314453));
#61121=CARTESIAN_POINT('Ctrl Pts',(-21.3472556036489,20.2900752735786,23.1515542935359));
#61122=CARTESIAN_POINT('Ctrl Pts',(-21.2530768665124,20.3578438856564,23.1574052726189));
#61123=CARTESIAN_POINT('Ctrl Pts',(-21.1588896618013,20.4256185907846,23.1632567777612));
#61124=CARTESIAN_POINT('Ctrl Pts',(-21.067715074096,20.4975573981569,23.1691082829035));
#61125=CARTESIAN_POINT('Ctrl Pts',(-20.9799312371807,20.5733518879087,23.1749597880458));
#61126=CARTESIAN_POINT('Ctrl Pts',(-20.8921182491639,20.6491715473607,23.1808132363455));
#61127=CARTESIAN_POINT('Ctrl Pts',(-20.8076985636316,20.7288491651498,23.1866666846453));
#61128=CARTESIAN_POINT('Ctrl Pts',(-20.7270149839343,20.8120380132683,23.1925201329451));
#61129=CARTESIAN_POINT('Ctrl Pts',(-20.6462396494869,20.895321465171,23.1983802378866));
#61130=CARTESIAN_POINT('Ctrl Pts',(-20.5692091892525,20.9821238204571,23.2042403428281));
#61131=CARTESIAN_POINT('Ctrl Pts',(-20.4962275378319,21.0720636089395,23.2101004477697));
#61132=CARTESIAN_POINT('Ctrl Pts',(-20.4231967378365,21.1620639662406,23.2159644991251));
#61133=CARTESIAN_POINT('Ctrl Pts',(-20.3542204213109,21.2552056324765,23.2218285504806));
#61134=CARTESIAN_POINT('Ctrl Pts',(-20.2895594209725,21.351077814285,23.227692601836));
#61135=CARTESIAN_POINT('Ctrl Pts',(-20.2248031232274,21.4470912925511,23.2335652956326));
#61136=CARTESIAN_POINT('Ctrl Pts',(-20.1643750497878,21.5458429667048,23.2394379894291));
#61137=CARTESIAN_POINT('Ctrl Pts',(-20.1084903520673,21.6468970475846,23.2453106832257));
#61138=CARTESIAN_POINT('Ctrl Pts',(-20.0931900566675,21.6745639645026,23.2469185285491));
#61139=CARTESIAN_POINT('Ctrl Pts',(-20.0782300418381,21.7024033481281,23.2485263738725));
#61140=CARTESIAN_POINT('Ctrl Pts',(-20.0636140872636,21.7304060112923,23.2501342191959));
#61141=CARTESIAN_POINT('Ctrl Pts',(-20.0102325682249,21.8326795021697,23.2560065161646));
#61142=CARTESIAN_POINT('Ctrl Pts',(-19.9612654151198,21.937475078632,23.2618788131334));
#61143=CARTESIAN_POINT('Ctrl Pts',(-19.9169590290309,22.0443749392236,23.2677511101021));
#61144=CARTESIAN_POINT('Ctrl Pts',(-19.8727100604997,22.1511362660858,23.2736157970404));
#61145=CARTESIAN_POINT('Ctrl Pts',(-19.833110004441,22.2599960757257,23.2794804839786));
#61146=CARTESIAN_POINT('Ctrl Pts',(-19.7983596049401,22.3705116846552,23.2853451709168));
#61147=CARTESIAN_POINT('Ctrl Pts',(-19.7636449440497,22.480913635199,23.2912038263917));
#61148=CARTESIAN_POINT('Ctrl Pts',(-19.73377014244,22.5929676059282,23.2970624818665));
#61149=CARTESIAN_POINT('Ctrl Pts',(-19.7088877586521,22.7062112528272,23.3029211373414));
#61150=CARTESIAN_POINT('Ctrl Pts',(-19.6830334470375,22.8238782963172,23.3090086370593));
#61151=CARTESIAN_POINT('Ctrl Pts',(-19.662569694719,22.9428294302189,23.3150961367772));
#61152=CARTESIAN_POINT('Ctrl Pts',(-19.6476105600349,23.0625285923154,23.3211836364951));
#61153=CARTESIAN_POINT('Ctrl Pts',(-19.6332304505008,23.177594543551,23.3270355065785));
#61154=CARTESIAN_POINT('Ctrl Pts',(-19.6239368024115,23.2933512432391,23.3328873766619));
#61155=CARTESIAN_POINT('Ctrl Pts',(-19.6197786264781,23.4093132525164,23.3387392467454));
#61156=CARTESIAN_POINT('Ctrl Pts',(-19.6156210836648,23.5252576055233,23.3445902258284));
#61157=CARTESIAN_POINT('Ctrl Pts',(-19.6165974731049,23.64140679296,23.3504412049114));
#61158=CARTESIAN_POINT('Ctrl Pts',(-19.6227047435426,23.7572727524113,23.3562921839944));
#61159=CARTESIAN_POINT('Ctrl Pts',(-19.6288125630827,23.8731491293273,23.3621436891367));
#61160=CARTESIAN_POINT('Ctrl Pts',(-19.6400521589127,23.9887418148016,23.367995194279));
#61161=CARTESIAN_POINT('Ctrl Pts',(-19.6563684495664,24.1035659645255,23.3738466994214));
#61162=CARTESIAN_POINT('Ctrl Pts',(-19.672690158505,24.2184282448499,23.3797001477212));
#61163=CARTESIAN_POINT('Ctrl Pts',(-19.6940918563675,24.332521072892,23.385553596021));
#61164=CARTESIAN_POINT('Ctrl Pts',(-19.7204671348071,24.4453686212546,23.3914070443208));
#61165=CARTESIAN_POINT('Ctrl Pts',(-19.7468724076655,24.5583445017839,23.3972671492624));
#61166=CARTESIAN_POINT('Ctrl Pts',(-19.77826245625,24.670071873261,23.4031272542039));
#61167=CARTESIAN_POINT('Ctrl Pts',(-19.8144806328283,24.7800888295989,23.4089873591455));
#61168=CARTESIAN_POINT('Ctrl Pts',(-19.8507232000819,24.8901798754717,23.414851410501));
#61169=CARTESIAN_POINT('Ctrl Pts',(-19.8918002234453,24.9985578270231,23.4207154618565));
#61170=CARTESIAN_POINT('Ctrl Pts',(-19.9375070867115,25.1047811900846,23.426579513212));
#61171=CARTESIAN_POINT('Ctrl Pts',(-19.9832813127701,25.2111611051785,23.4324522070086));
#61172=CARTESIAN_POINT('Ctrl Pts',(-20.0336988176947,25.3153797235017,23.4383249008052));
#61173=CARTESIAN_POINT('Ctrl Pts',(-20.0885092632119,25.417020472044,23.4441975946018));
#61174=CARTESIAN_POINT('Ctrl Pts',(-20.1035154463245,25.4448480087466,23.4458054399248));
#61175=CARTESIAN_POINT('Ctrl Pts',(-20.1188506646454,25.472482487263,23.4474132852478));
#61176=CARTESIAN_POINT('Ctrl Pts',(-20.1345092319351,25.4999157616267,23.4490211305708));
#61177=CARTESIAN_POINT('Ctrl Pts',(-20.1916986617359,25.6001096867417,23.4548934275394));
#61178=CARTESIAN_POINT('Ctrl Pts',(-20.2533961163809,25.6979530259088,23.4607657245081));
#61179=CARTESIAN_POINT('Ctrl Pts',(-20.3193832827261,25.7930126383646,23.4666380214768));
#61180=CARTESIAN_POINT('Ctrl Pts',(-20.3852849349444,25.8879490611122,23.472502708415));
#61181=CARTESIAN_POINT('Ctrl Pts',(-20.4554650102053,25.9801085946985,23.4783673953532));
#61182=CARTESIAN_POINT('Ctrl Pts',(-20.5296595821508,26.0690830605645,23.4842320822914));
#61183=CARTESIAN_POINT('Ctrl Pts',(-20.6037778496235,26.1579660217618,23.4900907377662));
#61184=CARTESIAN_POINT('Ctrl Pts',(-20.6819021385134,26.2436701150863,23.495949393241));
#61185=CARTESIAN_POINT('Ctrl Pts',(-20.763725935402,26.3258170739372,23.5018080487158));
#61186=CARTESIAN_POINT('Ctrl Pts',(-20.8487458418672,26.4111727653555,23.5078955484337));
#61187=CARTESIAN_POINT('Ctrl Pts',(-20.9377599009622,26.4926873940978,23.5139830481516));
#61188=CARTESIAN_POINT('Ctrl Pts',(-21.0303787679168,26.569975236617,23.5200705478695));
#61189=CARTESIAN_POINT('Ctrl Pts',(-21.1194126244761,26.6442714886755,23.5259224179529));
#61190=CARTESIAN_POINT('Ctrl Pts',(-21.2117770673393,26.7146617942,23.5317742880363));
#61191=CARTESIAN_POINT('Ctrl Pts',(-21.307090181013,26.7808425193724,23.5376261581197));
#61192=CARTESIAN_POINT('Ctrl Pts',(-21.4023887823984,26.8470131679275,23.5434771372026));
#61193=CARTESIAN_POINT('Ctrl Pts',(-21.5006348224522,26.9089752748323,23.5493281162856));
#61194=CARTESIAN_POINT('Ctrl Pts',(-21.6014160367423,26.9664675887337,23.5551790953685));
#61195=CARTESIAN_POINT('Ctrl Pts',(-21.7022063122337,27.0239650717476,23.5610306005108));
#61196=CARTESIAN_POINT('Ctrl Pts',(-21.8055318559913,27.0769917580158,23.5668821056531));
#61197=CARTESIAN_POINT('Ctrl Pts',(-21.9109549864961,27.1253319095972,23.5727336107954));
#61198=CARTESIAN_POINT('Ctrl Pts',(-22.0164131257273,27.1736881138906,23.5785870590951));
#61199=CARTESIAN_POINT('Ctrl Pts',(-22.1239698612128,27.2173545166911,23.5844405073949));
#61200=CARTESIAN_POINT('Ctrl Pts',(-22.2331673531572,27.2561634362463,23.5902939556947));
#61201=CARTESIAN_POINT('Ctrl Pts',(-22.3424890263619,27.2950164899703,23.5961540606362));
#61202=CARTESIAN_POINT('Ctrl Pts',(-22.4534547905528,27.3290008961693,23.6020141655777));
#61203=CARTESIAN_POINT('Ctrl Pts',(-22.5655913616488,27.3579987653874,23.6078742705193));
#61204=CARTESIAN_POINT('Ctrl Pts',(-22.6778034497074,27.3870161628556,23.6137383218747));
#61205=CARTESIAN_POINT('Ctrl Pts',(-22.7911875112451,27.411040251181,23.6196023732302));
#61206=CARTESIAN_POINT('Ctrl Pts',(-22.9052615060763,27.4300045310973,23.6254664245856));
#61207=CARTESIAN_POINT('Ctrl Pts',(-23.0195036232043,27.4489967605765,23.6313391183822));
#61208=CARTESIAN_POINT('Ctrl Pts',(-23.134437294166,27.4629142491113,23.6372118121788));
#61209=CARTESIAN_POINT('Ctrl Pts',(-23.2495767306492,27.4717424351194,23.6430845059753));
#61210=CARTESIAN_POINT('Ctrl Pts',(-23.2810999823131,27.4741594447711,23.6446923512988));
#61211=CARTESIAN_POINT('Ctrl Pts',(-23.3126386683647,27.4761952754471,23.6463001966222));
#61212=CARTESIAN_POINT('Ctrl Pts',(-23.3441828618122,27.4778503078361,23.6479080419457));
#61213=CARTESIAN_POINT('Ctrl Pts',(-23.4593910033285,27.4838949450528,23.6537803389143));
#61214=CARTESIAN_POINT('Ctrl Pts',(-23.5750583359852,27.4848763139783,23.659652635883));
#61215=CARTESIAN_POINT('Ctrl Pts',(-23.6907024436814,27.4807439541785,23.6655249328516));
#61216=CARTESIAN_POINT('Ctrl Pts',(-23.806196685798,27.4766169495888,23.6713896197898));
#61217=CARTESIAN_POINT('Ctrl Pts',(-23.9216673535017,27.4673894095967,23.6772543067279));
#61218=CARTESIAN_POINT('Ctrl Pts',(-24.0366283759371,27.4530627420602,23.6831189936661));
#61219=CARTESIAN_POINT('Ctrl Pts',(-24.1514711681574,27.4387508086044,23.6889776491408));
#61220=CARTESIAN_POINT('Ctrl Pts',(-24.2658049499038,27.4193502292692,23.6948363046156));
#61221=CARTESIAN_POINT('Ctrl Pts',(-24.3791457956417,27.3949144098029,23.7006949600903));
#61222=CARTESIAN_POINT('Ctrl Pts',(-24.4969138346452,27.3695241057051,23.7067824598082));
#61223=CARTESIAN_POINT('Ctrl Pts',(-24.6136093319937,27.3386971967743,23.7128699595262));
#61224=CARTESIAN_POINT('Ctrl Pts',(-24.7286973146415,27.302552745369,23.7189574592441));
#61225=CARTESIAN_POINT('Ctrl Pts',(-24.839330571942,27.2678073418933,23.7248093293275));
#61226=CARTESIAN_POINT('Ctrl Pts',(-24.9484780139794,27.2281485305923,23.7306611994108));
#61227=CARTESIAN_POINT('Ctrl Pts',(-25.0556777470133,27.1837334964278,23.7365130694942));
#61228=CARTESIAN_POINT('Ctrl Pts',(-25.162861157913,27.1393252248561,23.7423640485771));
#61229=CARTESIAN_POINT('Ctrl Pts',(-25.2680970676615,27.0901623285052,23.74821502766));
#61230=CARTESIAN_POINT('Ctrl Pts',(-25.3709428347095,27.0364504349272,23.7540660067429));
#61231=CARTESIAN_POINT('Ctrl Pts',(-25.4737978485814,26.9827337121332,23.7599175118852));
#61232=CARTESIAN_POINT('Ctrl Pts',(-25.5742619261146,26.9244673704379,23.7657690170274));
#61233=CARTESIAN_POINT('Ctrl Pts',(-25.671916977944,26.861903023144,23.7716205221696));
#61234=CARTESIAN_POINT('Ctrl Pts',(-25.7696044588906,26.7993178995921,23.7774739704694));
#61235=CARTESIAN_POINT('Ctrl Pts',(-25.8644807113959,26.732432155279,23.7833274187691));
#61236=CARTESIAN_POINT('Ctrl Pts',(-25.9561571801695,26.6615403394106,23.7891808670688));
#61237=CARTESIAN_POINT('Ctrl Pts',(-26.047937904995,26.590567904154,23.7950409720103));
#61238=CARTESIAN_POINT('Ctrl Pts',(-26.1365112558465,26.5155805571818,23.8009010769518));
#61239=CARTESIAN_POINT('Ctrl Pts',(-26.2215222202368,26.4369127560839,23.8067611818933));
#61240=CARTESIAN_POINT('Ctrl Pts',(-26.3065904341911,26.3581919771455,23.8126252332487));
#61241=CARTESIAN_POINT('Ctrl Pts',(-26.3880911947336,26.2757861019824,23.8184892846041));
#61242=CARTESIAN_POINT('Ctrl Pts',(-26.4657079917605,26.190064733418,23.8243533359595));
#61243=CARTESIAN_POINT('Ctrl Pts',(-26.5434391804522,26.1042170286681,23.830226029756));
#61244=CARTESIAN_POINT('Ctrl Pts',(-26.6172747186063,26.0150443954609,23.8360987235525));
#61245=CARTESIAN_POINT('Ctrl Pts',(-26.6869397661427,25.9229476645016,23.841971417349));
#61246=CARTESIAN_POINT('Ctrl Pts',(-26.7060128908106,25.8977331201467,23.8435792626729));
#61247=CARTESIAN_POINT('Ctrl Pts',(-26.7247736661513,25.8722995471868,23.8451871079967));
#61248=CARTESIAN_POINT('Ctrl Pts',(-26.7432170464849,25.8466555031449,23.8467949533206));
#61249=CARTESIAN_POINT('Ctrl Pts',(-26.811152181329,25.7521971360545,23.8527173594581));
#61250=CARTESIAN_POINT('Ctrl Pts',(-26.8750041066385,25.6545661064609,23.8586397655956));
#61251=CARTESIAN_POINT('Ctrl Pts',(-26.9344653447686,25.5541468991256,23.8645621717331));
#61252=CARTESIAN_POINT('Ctrl Pts',(-26.9938469440751,25.4538621872664,23.8704766457543));
#61253=CARTESIAN_POINT('Ctrl Pts',(-27.0488493477093,25.3507970685784,23.8763911197755));
#61254=CARTESIAN_POINT('Ctrl Pts',(-27.0992066329202,25.2453672143606,23.8823055937967));
#61255=CARTESIAN_POINT('Ctrl Pts',(-27.1495079646061,25.1400545064893,23.8882134960643));
#61256=CARTESIAN_POINT('Ctrl Pts',(-27.1951742719672,25.0323826519989,23.8941213983319));
#61257=CARTESIAN_POINT('Ctrl Pts',(-27.2359844121268,24.9227937899311,23.9000293005995));
#61258=CARTESIAN_POINT('Ctrl Pts',(-27.2767543114318,24.8133129880036,23.9059313773778));
#61259=CARTESIAN_POINT('Ctrl Pts',(-27.3126774360233,24.7019193187062,23.911833454156));
#61260=CARTESIAN_POINT('Ctrl Pts',(-27.3435801479668,24.589076191236,23.9177355309343));
#61261=CARTESIAN_POINT('Ctrl Pts',(-27.3744644883382,24.4763001486755,23.9236340989452));
#61262=CARTESIAN_POINT('Ctrl Pts',(-27.4003342475389,24.3620767509935,23.929532666956));
#61263=CARTESIAN_POINT('Ctrl Pts',(-27.4210652880595,24.2468855808382,23.9354312349669));
#61264=CARTESIAN_POINT('Ctrl Pts',(-27.4418044325967,24.1316493810493,23.9413321087999));
#61265=CARTESIAN_POINT('Ctrl Pts',(-27.4574007443461,24.0154450455376,23.9472329826329));
#61266=CARTESIAN_POINT('Ctrl Pts',(-27.4677809366463,23.8987639323588,23.953133856466));
#61267=CARTESIAN_POINT('Ctrl Pts',(-27.4781611289466,23.7820828191799,23.959034730299));
#61268=CARTESIAN_POINT('Ctrl Pts',(-27.4833251596027,23.6649253317523,23.9649356041321));
#61269=CARTESIAN_POINT('Ctrl Pts',(-27.4832517595538,23.5477880529337,23.9708364779651));
#61270=CARTESIAN_POINT('',(-27.4850558412115,23.5481778231382,25.2208358612592));
#61271=CARTESIAN_POINT('Ctrl Pts',(-27.4783256425004,23.5477610787469,23.9708379942064));
#61272=CARTESIAN_POINT('Ctrl Pts',(-27.481139687066,23.0531416688158,23.9957859510361));
#61273=CARTESIAN_POINT('Ctrl Pts',(-27.1646539659434,21.2476181443352,24.0870295449907));
#61274=CARTESIAN_POINT('Ctrl Pts',(-24.4510434083163,18.9863368193904,24.2445687760702));
#61275=CARTESIAN_POINT('Ctrl Pts',(-20.1974693245192,20.3254121329573,24.4434556874452));
#61276=CARTESIAN_POINT('Ctrl Pts',(-19.0248187389452,24.6278423513666,24.64234259882));
#61277=CARTESIAN_POINT('Ctrl Pts',(-22.0106581154577,27.9400588904565,24.841229510195));
#61278=CARTESIAN_POINT('Ctrl Pts',(-26.2772539213587,27.2403899709072,25.0340602178841));
#61279=CARTESIAN_POINT('Ctrl Pts',(-27.4807589030166,24.7347075626642,25.1605952884482));
#61280=CARTESIAN_POINT('Ctrl Pts',(-27.4883884996962,23.5481984972521,25.2208347218874));
#61281=CARTESIAN_POINT('',(-27.4832675014334,23.5537273857095,26.4708364861422));
#61282=CARTESIAN_POINT('Ctrl Pts',(-27.4832519785574,23.5481666328942,25.2208364779651));
#61283=CARTESIAN_POINT('Ctrl Pts',(-27.4831888029344,23.4290478671883,25.2268920962917));
#61284=CARTESIAN_POINT('Ctrl Pts',(-27.4777145063877,23.3100758243375,25.2329477146182));
#61285=CARTESIAN_POINT('Ctrl Pts',(-27.4668658374458,23.1916033811171,25.2390033329447));
#61286=CARTESIAN_POINT('Ctrl Pts',(-27.4563455896034,23.0767174470138,25.2448756299034));
#61287=CARTESIAN_POINT('Ctrl Pts',(-27.4407485117847,22.9621023256229,25.2507479268621));
#61288=CARTESIAN_POINT('Ctrl Pts',(-27.4200937657703,22.8482426862899,25.2566202238209));
#61289=CARTESIAN_POINT('Ctrl Pts',(-27.3994657866663,22.7345306000068,25.2624849107491));
#61290=CARTESIAN_POINT('Ctrl Pts',(-27.3737932466934,22.6215724518033,25.2683495976774));
#61291=CARTESIAN_POINT('Ctrl Pts',(-27.3431471645599,22.5098490984151,25.2742142846057));
#61292=CARTESIAN_POINT('Ctrl Pts',(-27.3125326000033,22.3982406455016,25.2800729400706));
#61293=CARTESIAN_POINT('Ctrl Pts',(-27.2769547759334,22.2878648577489,25.2859315955355));
#61294=CARTESIAN_POINT('Ctrl Pts',(-27.2365358654385,22.1791930204553,25.2917902510004));
#61295=CARTESIAN_POINT('Ctrl Pts',(-27.1945381566028,22.0662763652207,25.2978777507221));
#61296=CARTESIAN_POINT('Ctrl Pts',(-27.1473135383742,21.9551999371496,25.3039652504437));
#61297=CARTESIAN_POINT('Ctrl Pts',(-27.0950564754956,21.8464761379119,25.3100527501653));
#61298=CARTESIAN_POINT('Ctrl Pts',(-27.0448221335849,21.741960724992,25.315904620239));
#61299=CARTESIAN_POINT('Ctrl Pts',(-26.989937881809,21.6396196077161,25.3217564903127));
#61300=CARTESIAN_POINT('Ctrl Pts',(-26.9306254464183,21.5398874013262,25.3276083603864));
#61301=CARTESIAN_POINT('Ctrl Pts',(-26.8713220418845,21.4401703800702,25.3334593394597));
#61302=CARTESIAN_POINT('Ctrl Pts',(-26.8075920055672,21.3430618350799,25.339310318533));
#61303=CARTESIAN_POINT('Ctrl Pts',(-26.7397022490512,21.2489703889635,25.3451612976064));
#61304=CARTESIAN_POINT('Ctrl Pts',(-26.6718063885919,21.1548704831194,25.3510128027391));
#61305=CARTESIAN_POINT('Ctrl Pts',(-26.599750306352,21.0637885506526,25.3568643078719));
#61306=CARTESIAN_POINT('Ctrl Pts',(-26.5238429085688,20.9761023281205,25.3627158130046));
#61307=CARTESIAN_POINT('Ctrl Pts',(-26.4479103035901,20.8883869869013,25.3685692612949));
#61308=CARTESIAN_POINT('Ctrl Pts',(-26.3681241103962,20.8040699102383,25.3744227095852));
#61309=CARTESIAN_POINT('Ctrl Pts',(-26.2848314978683,20.723493454985,25.3802761578756));
#61310=CARTESIAN_POINT('Ctrl Pts',(-26.2014441635507,20.6428253668026,25.3861362628078));
#61311=CARTESIAN_POINT('Ctrl Pts',(-26.1145427481355,20.5659066782754,25.3919963677401));
#61312=CARTESIAN_POINT('Ctrl Pts',(-26.0245091126335,20.4930408328289,25.3978564726723));
#61313=CARTESIAN_POINT('Ctrl Pts',(-25.9344148451114,20.4201259167948,25.4037205240186));
#61314=CARTESIAN_POINT('Ctrl Pts',(-25.8411844890698,20.3512695234804,25.4095845753648));
#61315=CARTESIAN_POINT('Ctrl Pts',(-25.7452291732017,20.2867319567266,25.4154486267111));
#61316=CARTESIAN_POINT('Ctrl Pts',(-25.6491324383487,20.22209927448,25.4213213204987));
#61317=CARTESIAN_POINT('Ctrl Pts',(-25.5503030799719,20.161798336786,25.4271940142863));
#61318=CARTESIAN_POINT('Ctrl Pts',(-25.4491771637542,20.106043734052,25.4330667080738));
#61319=CARTESIAN_POINT('Ctrl Pts',(-25.4214905778971,20.0907790555872,25.4346745534892));
#61320=CARTESIAN_POINT('Ctrl Pts',(-25.3936319633703,20.0758548794012,25.4362823989045));
#61321=CARTESIAN_POINT('Ctrl Pts',(-25.3656105122009,20.0612749733527,25.4378902443198));
#61322=CARTESIAN_POINT('Ctrl Pts',(-25.2632684082845,20.0080251166311,25.443762541282));
#61323=CARTESIAN_POINT('Ctrl Pts',(-25.1584099018201,19.9591928679016,25.4496348382441));
#61324=CARTESIAN_POINT('Ctrl Pts',(-25.0514531110148,19.9150240903652,25.4555071352063));
#61325=CARTESIAN_POINT('Ctrl Pts',(-24.9446349277183,19.8709125520575,25.4613718221378));
#61326=CARTESIAN_POINT('Ctrl Pts',(-24.8357242461717,19.831452622943,25.4672365090693));
#61327=CARTESIAN_POINT('Ctrl Pts',(-24.7251640078375,19.796844477242,25.4731011960008));
#61328=CARTESIAN_POINT('Ctrl Pts',(-24.6147174737893,19.7622719238529,25.4789598514688));
#61329=CARTESIAN_POINT('Ctrl Pts',(-24.5026251494462,19.7325413517449,25.4848185069368));
#61330=CARTESIAN_POINT('Ctrl Pts',(-24.3893495747704,19.7078047243322,25.4906771624049));
#61331=CARTESIAN_POINT('Ctrl Pts',(-24.2716493561908,19.6821018624247,25.4967646621253));
#61332=CARTESIAN_POINT('Ctrl Pts',(-24.1526719854879,19.6617912078772,25.5028521618457));
#61333=CARTESIAN_POINT('Ctrl Pts',(-24.0329536712201,19.6469861290642,25.5089396615661));
#61334=CARTESIAN_POINT('Ctrl Pts',(-23.9178693093251,19.6327541123638,25.5147915316425));
#61335=CARTESIAN_POINT('Ctrl Pts',(-23.8021007454281,19.6236094418233,25.5206434017189));
#61336=CARTESIAN_POINT('Ctrl Pts',(-23.6861334810624,19.6196005033917,25.5264952717952));
#61337=CARTESIAN_POINT('Ctrl Pts',(-23.5701838737685,19.6155921753574,25.5323462508711));
#61338=CARTESIAN_POINT('Ctrl Pts',(-23.4540360391832,19.6167180389193,25.538197229947));
#61339=CARTESIAN_POINT('Ctrl Pts',(-23.3381780353898,19.622974414726,25.5440482090229));
#61340=CARTESIAN_POINT('Ctrl Pts',(-23.222309614848,19.6292313530411,25.5498997141581));
#61341=CARTESIAN_POINT('Ctrl Pts',(-23.1067314897063,19.6406196982961,25.5557512192932));
#61342=CARTESIAN_POINT('Ctrl Pts',(-22.9919284329852,19.6570837451142,25.5616027244284));
#61343=CARTESIAN_POINT('Ctrl Pts',(-22.8770872526689,19.6735532592837,25.5674561727209));
#61344=CARTESIAN_POINT('Ctrl Pts',(-22.7630220615436,19.6951017679341,25.5733096210135));
#61345=CARTESIAN_POINT('Ctrl Pts',(-22.6502085496725,19.7216222504544,25.5791630693061));
#61346=CARTESIAN_POINT('Ctrl Pts',(-22.5372667443421,19.748172892522,25.5850231742404));
#61347=CARTESIAN_POINT('Ctrl Pts',(-22.4255798620429,19.7797066994432,25.5908832791747));
#61348=CARTESIAN_POINT('Ctrl Pts',(-22.3156096068854,19.8160664291787,25.5967433841091));
#61349=CARTESIAN_POINT('Ctrl Pts',(-22.2055652936444,19.8524506449164,25.6026074354572));
#61350=CARTESIAN_POINT('Ctrl Pts',(-22.0972402948686,19.8936671081312,25.6084714868054));
#61351=CARTESIAN_POINT('Ctrl Pts',(-21.9910758410352,19.9395106346174,25.6143355381536));
#61352=CARTESIAN_POINT('Ctrl Pts',(-21.8847549219887,19.9854217253107,25.620208231943));
#61353=CARTESIAN_POINT('Ctrl Pts',(-21.7806012734547,20.0359733095945,25.6260809257323));
#61354=CARTESIAN_POINT('Ctrl Pts',(-21.6790311459315,20.0909145133063,25.6319536195216));
#61355=CARTESIAN_POINT('Ctrl Pts',(-21.6512229428726,20.1059564964796,25.6335614649126));
#61356=CARTESIAN_POINT('Ctrl Pts',(-21.6236082212991,20.1213272661659,25.6351693103035));
#61357=CARTESIAN_POINT('Ctrl Pts',(-21.5961951198538,20.1370211256463,25.6367771556945));
#61358=CARTESIAN_POINT('Ctrl Pts',(-21.4960748752334,20.1943394503662,25.6426494527118));
#61359=CARTESIAN_POINT('Ctrl Pts',(-21.3983110161499,20.2561627712394,25.6485217497292));
#61360=CARTESIAN_POINT('Ctrl Pts',(-21.3033364020601,20.3222722178772,25.6543940467465));
#61361=CARTESIAN_POINT('Ctrl Pts',(-21.2084848675243,20.3882959919246,25.6602587337335));
#61362=CARTESIAN_POINT('Ctrl Pts',(-21.1164157259102,20.4585946118878,25.6661234207205));
#61363=CARTESIAN_POINT('Ctrl Pts',(-21.0275368157894,20.5329036263259,25.6719881077075));
#61364=CARTESIAN_POINT('Ctrl Pts',(-20.9387493120618,20.6071362185963,25.6778467632312));
#61365=CARTESIAN_POINT('Ctrl Pts',(-20.8531458290784,20.6853707380602,25.6837054187549));
#61366=CARTESIAN_POINT('Ctrl Pts',(-20.7711042386705,20.7673001847462,25.6895640742786));
#61367=CARTESIAN_POINT('Ctrl Pts',(-20.6858580324472,20.8524298668164,25.6956515739783));
#61368=CARTESIAN_POINT('Ctrl Pts',(-20.6044580258697,20.9415487550151,25.7017390736779));
#61369=CARTESIAN_POINT('Ctrl Pts',(-20.5272894410991,21.0342670085045,25.7078265733775));
#61370=CARTESIAN_POINT('Ctrl Pts',(-20.453107829823,21.1233964056421,25.7136784435097));
#61371=CARTESIAN_POINT('Ctrl Pts',(-20.382836448119,21.2158513597159,25.7195303136419));
#61372=CARTESIAN_POINT('Ctrl Pts',(-20.3167784380616,21.3112495647897,25.725382183774));
#61373=CARTESIAN_POINT('Ctrl Pts',(-20.2507304859382,21.4066332446175,25.7312331629057));
#61374=CARTESIAN_POINT('Ctrl Pts',(-20.1888948651744,21.5049589446407,25.7370841420373));
#61375=CARTESIAN_POINT('Ctrl Pts',(-20.1315322963575,21.6058140645527,25.7429351211689));
#61376=CARTESIAN_POINT('Ctrl Pts',(-20.0741645700954,21.7066782523076,25.7487866263597));
#61377=CARTESIAN_POINT('Ctrl Pts',(-20.0212708996425,21.8100719526892,25.7546381315505));
#61378=CARTESIAN_POINT('Ctrl Pts',(-19.973066459502,21.915557206897,25.7604896367413));
#61379=CARTESIAN_POINT('Ctrl Pts',(-19.9248460117182,22.021077490457,25.7663430850893));
#61380=CARTESIAN_POINT('Ctrl Pts',(-19.8813180623491,22.1286903331453,25.7721965334374));
#61381=CARTESIAN_POINT('Ctrl Pts',(-19.8426497038071,22.2379376797462,25.7780499817854));
#61382=CARTESIAN_POINT('Ctrl Pts',(-19.8039373709488,22.347309264291,25.7839100867746));
#61383=CARTESIAN_POINT('Ctrl Pts',(-19.7700957974783,22.4583186729053,25.7897701917639));
#61384=CARTESIAN_POINT('Ctrl Pts',(-19.7412422636771,22.5704924701789,25.7956302967531));
#61385=CARTESIAN_POINT('Ctrl Pts',(-19.7123692988283,22.6827418094784,25.801494348156));
#61386=CARTESIAN_POINT('Ctrl Pts',(-19.6884911473059,22.7961566952951,25.8073583995588));
#61387=CARTESIAN_POINT('Ctrl Pts',(-19.6696736879759,22.9102550022567,25.8132224509617));
#61388=CARTESIAN_POINT('Ctrl Pts',(-19.6508284954699,23.0245214673303,25.8190951448049));
#61389=CARTESIAN_POINT('Ctrl Pts',(-19.6370589297637,23.1394729548704,25.8249678386481));
#61390=CARTESIAN_POINT('Ctrl Pts',(-19.6283789272586,23.2546236582208,25.8308405324914));
#61391=CARTESIAN_POINT('Ctrl Pts',(-19.626002488476,23.2861499852147,25.8324483773507));
#61392=CARTESIAN_POINT('Ctrl Pts',(-19.6240072479966,23.3176912560264,25.8340562222101));
#61393=CARTESIAN_POINT('Ctrl Pts',(-19.6223928123571,23.3492375441713,25.8356640670695));
#61394=CARTESIAN_POINT('Ctrl Pts',(-19.6164964441009,23.4644533678718,25.8415363639624));
#61395=CARTESIAN_POINT('Ctrl Pts',(-19.615663930763,23.580121866316,25.8474086608553));
#61396=CARTESIAN_POINT('Ctrl Pts',(-19.619945111908,23.6957605588742,25.8532809577482));
#61397=CARTESIAN_POINT('Ctrl Pts',(-19.6242207449823,23.811249392871,25.8591456446107));
#61398=CARTESIAN_POINT('Ctrl Pts',(-19.6335968787783,23.9267080885084,25.8650103314732));
#61399=CARTESIAN_POINT('Ctrl Pts',(-19.6480714799083,24.0416505771553,25.8708750183357));
#61400=CARTESIAN_POINT('Ctrl Pts',(-19.6625311948174,24.1564748546504,25.8767336737351));
#61401=CARTESIAN_POINT('Ctrl Pts',(-19.6820788962216,24.2707835734378,25.8825923291344));
#61402=CARTESIAN_POINT('Ctrl Pts',(-19.7066605556467,24.3840928771222,25.8884509845337));
#61403=CARTESIAN_POINT('Ctrl Pts',(-19.7322023967884,24.5018281440757,25.89453848428));
#61404=CARTESIAN_POINT('Ctrl Pts',(-19.7631794580564,24.6184838737862,25.9006259840263));
#61405=CARTESIAN_POINT('Ctrl Pts',(-19.7994719887203,24.7335252468569,25.9067134837726));
#61406=CARTESIAN_POINT('Ctrl Pts',(-19.8343597391252,24.8441136967807,25.9125653537814));
#61407=CARTESIAN_POINT('Ctrl Pts',(-19.8741589810529,24.953210009544,25.9184172237903));
#61408=CARTESIAN_POINT('Ctrl Pts',(-19.9187119352538,25.0603524940826,25.9242690937992));
#61409=CARTESIAN_POINT('Ctrl Pts',(-19.9632581058659,25.1674786652122,25.9301200728081));
#61410=CARTESIAN_POINT('Ctrl Pts',(-20.0125563909366,25.2726512180256,25.935971051817));
#61411=CARTESIAN_POINT('Ctrl Pts',(-20.0664005934423,25.3754277759758,25.9418220308259));
#61412=CARTESIAN_POINT('Ctrl Pts',(-20.1202496370651,25.4782135745374,25.9476735358947));
#61413=CARTESIAN_POINT('Ctrl Pts',(-20.1786452187761,25.5786025837979,25.9535250409634));
#61414=CARTESIAN_POINT('Ctrl Pts',(-20.2413351874361,25.6761770385543,25.9593765460322));
#61415=CARTESIAN_POINT('Ctrl Pts',(-20.304045974077,25.7737838956739,25.9652299942591));
#61416=CARTESIAN_POINT('Ctrl Pts',(-20.3710537599934,25.8685739921877,25.971083442486));
#61417=CARTESIAN_POINT('Ctrl Pts',(-20.4420634961868,25.9601591521987,25.9769368907129));
#61418=CARTESIAN_POINT('Ctrl Pts',(-20.5131539858863,26.0518484644455,25.9827969955829));
#61419=CARTESIAN_POINT('Ctrl Pts',(-20.5882552562493,26.1403252385755,25.9886571004528));
#61420=CARTESIAN_POINT('Ctrl Pts',(-20.6670323930936,26.2252348928264,25.9945172053228));
#61421=CARTESIAN_POINT('Ctrl Pts',(-20.7458625814187,26.3102017284253,26.0003812566073));
#61422=CARTESIAN_POINT('Ctrl Pts',(-20.8283732718001,26.391596371224,26.0062453078918));
#61423=CARTESIAN_POINT('Ctrl Pts',(-20.9141944544012,26.469102787041,26.0121093591763));
#61424=CARTESIAN_POINT('Ctrl Pts',(-21.0001421203178,26.5467234318648,26.0179820529035));
#61425=CARTESIAN_POINT('Ctrl Pts',(-21.0894096984637,26.6204441505506,26.0238547466307));
#61426=CARTESIAN_POINT('Ctrl Pts',(-21.181596004773,26.6899906190947,26.0297274403578));
#61427=CARTESIAN_POINT('Ctrl Pts',(-21.2068350847242,26.7090312873912,26.0313352863866));
#61428=CARTESIAN_POINT('Ctrl Pts',(-21.2322927913215,26.7277593244731,26.0329431324155));
#61429=CARTESIAN_POINT('Ctrl Pts',(-21.257960560544,26.7461696956708,26.0345509784443));
#61430=CARTESIAN_POINT('Ctrl Pts',(-21.3517063298641,26.8134094466769,26.0404232753943));
#61431=CARTESIAN_POINT('Ctrl Pts',(-21.4485701703373,26.8766335814062,26.0462955723443));
#61432=CARTESIAN_POINT('Ctrl Pts',(-21.5481731033077,26.9355393677587,26.0521678692943));
#61433=CARTESIAN_POINT('Ctrl Pts',(-21.6476469587745,26.9943688168827,26.058032556213));
#61434=CARTESIAN_POINT('Ctrl Pts',(-21.749852495235,27.0488908380479,26.0638972431318));
#61435=CARTESIAN_POINT('Ctrl Pts',(-21.8543796758573,27.0988444012723,26.0697619300506));
#61436=CARTESIAN_POINT('Ctrl Pts',(-21.958799356805,27.1487465903779,26.0756205855053));
#61437=CARTESIAN_POINT('Ctrl Pts',(-22.0655355619873,27.1940894896742,26.08147924096));
#61438=CARTESIAN_POINT('Ctrl Pts',(-22.1741520102149,27.2346570093248,26.0873378964147));
#61439=CARTESIAN_POINT('Ctrl Pts',(-22.287011113101,27.2768091322196,26.0934253961399));
#61440=CARTESIAN_POINT('Ctrl Pts',(-22.4018999500598,27.3138049776414,26.0995128958651));
#61441=CARTESIAN_POINT('Ctrl Pts',(-22.5183038382273,27.3454562013346,26.1056003955903));
#61442=CARTESIAN_POINT('Ctrl Pts',(-22.6302020655757,27.3758822968923,26.111452265652));
#61443=CARTESIAN_POINT('Ctrl Pts',(-22.743499802301,27.4013697087658,26.1173041357137));
#61444=CARTESIAN_POINT('Ctrl Pts',(-22.8577233335861,27.4218016156873,26.1231560057754));
#61445=CARTESIAN_POINT('Ctrl Pts',(-22.9719294732892,27.4422304116632,26.1290069848361));
#61446=CARTESIAN_POINT('Ctrl Pts',(-23.0870607204648,27.4576051604215,26.1348579638968));
#61447=CARTESIAN_POINT('Ctrl Pts',(-23.2026334380633,27.4678602156951,26.1407089429576));
#61448=CARTESIAN_POINT('Ctrl Pts',(-23.3182165467511,27.4781161929961,26.1465604480771));
#61449=CARTESIAN_POINT('Ctrl Pts',(-23.4342407929771,27.483251525221,26.1524119531966));
#61450=CARTESIAN_POINT('Ctrl Pts',(-23.5502184054799,27.4832525315461,26.1582634583162));
#61451=CARTESIAN_POINT('Ctrl Pts',(-23.6662345316134,27.4832535382055,26.1641169065927));
#61452=CARTESIAN_POINT('Ctrl Pts',(-23.7822035800667,27.4781168286814,26.1699703548692));
#61453=CARTESIAN_POINT('Ctrl Pts',(-23.8976394854457,27.4678808071133,26.1758238031457));
#61454=CARTESIAN_POINT('Ctrl Pts',(-24.0132066665041,27.4576331449669,26.1816839080634));
#61455=CARTESIAN_POINT('Ctrl Pts',(-24.1282390823215,27.4422746326328,26.1875440129811));
#61456=CARTESIAN_POINT('Ctrl Pts',(-24.2422573819904,27.4218953725521,26.1934041178988));
#61457=CARTESIAN_POINT('Ctrl Pts',(-24.356352465841,27.4015023883165,26.19926816923));
#61458=CARTESIAN_POINT('Ctrl Pts',(-24.4694316713346,27.3760820142201,26.2051322205612));
#61459=CARTESIAN_POINT('Ctrl Pts',(-24.5810291076006,27.345774715869,26.2109962718924));
#61460=CARTESIAN_POINT('Ctrl Pts',(-24.6927910162044,27.3154227506116,26.2168689656644));
#61461=CARTESIAN_POINT('Ctrl Pts',(-24.8030664047997,27.2801696120006,26.2227416594364));
#61462=CARTESIAN_POINT('Ctrl Pts',(-24.9114076229943,27.2402045391636,26.2286143532083));
#61463=CARTESIAN_POINT('Ctrl Pts',(-24.9410696402747,27.2292627692551,26.2302221987453));
#61464=CARTESIAN_POINT('Ctrl Pts',(-24.9705868127282,27.2179680748707,26.2318300442823));
#61465=CARTESIAN_POINT('Ctrl Pts',(-24.9999502753945,27.2063249396082,26.2334378898193));
#61466=CARTESIAN_POINT('Ctrl Pts',(-25.1071937747825,27.163800984461,26.2393101870964));
#61467=CARTESIAN_POINT('Ctrl Pts',(-25.2127443181152,27.1164831324113,26.2451824843735));
#61468=CARTESIAN_POINT('Ctrl Pts',(-25.3161423577351,27.0645265850778,26.2510547816507));
#61469=CARTESIAN_POINT('Ctrl Pts',(-25.4194064017332,27.0126373692904,26.2569194688983));
#61470=CARTESIAN_POINT('Ctrl Pts',(-25.5205231233169,26.9561215965882,26.262784156146));
#61471=CARTESIAN_POINT('Ctrl Pts',(-25.6190512712638,26.8951831401157,26.2686488433937));
#61472=CARTESIAN_POINT('Ctrl Pts',(-25.7174780891955,26.8343073550204,26.2745074991787));
#61473=CARTESIAN_POINT('Ctrl Pts',(-25.813321279255,26.7690181493974,26.2803661549637));
#61474=CARTESIAN_POINT('Ctrl Pts',(-25.9061632129341,26.6995657682618,26.2862248107487));
#61475=CARTESIAN_POINT('Ctrl Pts',(-26.0026316273711,26.627400521142,26.2923123103506));
#61476=CARTESIAN_POINT('Ctrl Pts',(-26.0958591363951,26.5507404384385,26.2983998099525));
#61477=CARTESIAN_POINT('Ctrl Pts',(-26.1854090749907,26.4699167233987,26.3044873095544));
#61478=CARTESIAN_POINT('Ctrl Pts',(-26.2714927987967,26.3922214566954,26.3103391799478));
#61479=CARTESIAN_POINT('Ctrl Pts',(-26.354178018873,26.3106791910452,26.3161910503412));
#61480=CARTESIAN_POINT('Ctrl Pts',(-26.433110388563,26.2256253238654,26.3220429207346));
#61481=CARTESIAN_POINT('Ctrl Pts',(-26.5120307400745,26.1405844069182,26.3278939001269));
#61482=CARTESIAN_POINT('Ctrl Pts',(-26.5871990962165,26.0520332544666,26.3337448795193));
#61483=CARTESIAN_POINT('Ctrl Pts',(-26.6582988013325,25.9603432739251,26.3395958589117));
#61484=CARTESIAN_POINT('Ctrl Pts',(-26.7294048989848,25.8686450495868,26.3454473643625));
#61485=CARTESIAN_POINT('Ctrl Pts',(-26.7964413650836,25.7738077628449,26.3512988698133));
#61486=CARTESIAN_POINT('Ctrl Pts',(-26.8591330286557,25.67623438882,26.3571503752641));
#61487=CARTESIAN_POINT('Ctrl Pts',(-26.9218455107501,25.5786286128239,26.3630038238711));
#61488=CARTESIAN_POINT('Ctrl Pts',(-26.9802100980387,25.4782852904618,26.3688572724781));
#61489=CARTESIAN_POINT('Ctrl Pts',(-27.0339963615948,25.3756341158102,26.3747107210852));
#61490=CARTESIAN_POINT('Ctrl Pts',(-27.0878437917777,25.2728662045481,26.3805708263306));
#61491=CARTESIAN_POINT('Ctrl Pts',(-27.1371023141482,25.1677855688989,26.386430931576));
#61492=CARTESIAN_POINT('Ctrl Pts',(-27.1815886238932,25.0608441990527,26.3922910368214));
#61493=CARTESIAN_POINT('Ctrl Pts',(-27.2261048923698,24.9538308109199,26.3981550884792));
#61494=CARTESIAN_POINT('Ctrl Pts',(-27.265842407552,24.844954580822,26.4040191401369));
#61495=CARTESIAN_POINT('Ctrl Pts',(-27.300667511722,24.7346833982218,26.4098831917946));
#61496=CARTESIAN_POINT('Ctrl Pts',(-27.3355439411133,24.624249698007,26.4157558858888));
#61497=CARTESIAN_POINT('Ctrl Pts',(-27.3654934034944,24.5124173399615,26.421628579983));
#61498=CARTESIAN_POINT('Ctrl Pts',(-27.3904331348813,24.3996652316849,26.4275012740772));
#61499=CARTESIAN_POINT('Ctrl Pts',(-27.397261203266,24.3687956487736,26.4291091164495));
#61500=CARTESIAN_POINT('Ctrl Pts',(-27.4037140570737,24.3378571558806,26.4307169588218));
#61501=CARTESIAN_POINT('Ctrl Pts',(-27.4097906765489,24.3068596347614,26.4323248011941));
#61502=CARTESIAN_POINT('Ctrl Pts',(-27.4421880595738,24.1415969309467,26.4408969827157));
#61503=CARTESIAN_POINT('Ctrl Pts',(-27.4639789012828,23.9741922082478,26.4494691642373));
#61504=CARTESIAN_POINT('Ctrl Pts',(-27.4749442882531,23.8057591186902,26.4580413457589));
#61505=CARTESIAN_POINT('Ctrl Pts',(-27.4804000591723,23.7219561161772,26.4623063898276));
#61506=CARTESIAN_POINT('Ctrl Pts',(-27.4831766269209,23.6378988905708,26.4665714338964));
#61507=CARTESIAN_POINT('Ctrl Pts',(-27.483250996526,23.5537275325671,26.4708364779651));
#61508=CARTESIAN_POINT('',(-27.4767779762767,23.5507168464414,27.7208364779651));
#61509=CARTESIAN_POINT('Ctrl Pts',(-27.4848126564242,23.5537136372146,26.4708372516642));
#61510=CARTESIAN_POINT('Ctrl Pts',(-27.4750743970666,22.4982795966798,26.5242954052991));
#61511=CARTESIAN_POINT('Ctrl Pts',(-26.4929708527558,20.1179887131869,26.6440491960592));
#61512=CARTESIAN_POINT('Ctrl Pts',(-22.4668397420095,19.0262093874363,26.8300986239438));
#61513=CARTESIAN_POINT('Ctrl Pts',(-19.1584684333861,22.0163084907552,27.0289855353188));
#61514=CARTESIAN_POINT('Ctrl Pts',(-19.8857744770669,26.4159729476211,27.2278724466937));
#61515=CARTESIAN_POINT('Ctrl Pts',(-23.9804249150498,28.1822817349765,27.4267593580686));
#61516=CARTESIAN_POINT('Ctrl Pts',(-27.036853459589,26.124923812395,27.5910807018257));
#61517=CARTESIAN_POINT('Ctrl Pts',(-27.4774395641842,24.1804189441493,27.6891064084579));
#61518=CARTESIAN_POINT('Ctrl Pts',(-27.4767779762767,23.5507168464414,27.7208364779651));
#61519=CARTESIAN_POINT('',(-27.4832508103722,23.5465728691724,28.9708364828311));
#61520=CARTESIAN_POINT('Ctrl Pts',(-27.4767779762767,23.5507168464414,27.7208364779651));
#61521=CARTESIAN_POINT('Ctrl Pts',(-27.4760572668075,22.8647426025963,27.7554020455828));
#61522=CARTESIAN_POINT('Ctrl Pts',(-26.9778217625069,20.8621128540598,27.8562632503257));
#61523=CARTESIAN_POINT('Ctrl Pts',(-23.7820353409766,18.9040740354896,28.0234200921932));
#61524=CARTESIAN_POINT('Ctrl Pts',(-19.766626082321,20.8437801165488,28.2223070035682));
#61525=CARTESIAN_POINT('Ctrl Pts',(-19.2280545259956,25.2705428060829,28.4211939149431));
#61526=CARTESIAN_POINT('Ctrl Pts',(-22.6612055347411,28.1164329704806,28.6200808263178));
#61527=CARTESIAN_POINT('Ctrl Pts',(-26.5764164330689,26.8729013389392,28.803295013992));
#61528=CARTESIAN_POINT('Ctrl Pts',(-27.4738633797249,24.5471524573527,28.920213564541));
#61529=CARTESIAN_POINT('Ctrl Pts',(-27.4830944336655,23.5465731116532,28.9708364779651));
#61530=CARTESIAN_POINT('',(-25.2989497345943,27.0731131722205,29.9999401439846));
#61531=CARTESIAN_POINT('Ctrl Pts',(-27.4832508103721,23.5465728691724,28.9708364828311));
#61532=CARTESIAN_POINT('Ctrl Pts',(-27.483105894416,23.391679804188,28.9786728438705));
#61533=CARTESIAN_POINT('Ctrl Pts',(-27.4738070756413,23.2371955920286,28.9865092049099));
#61534=CARTESIAN_POINT('Ctrl Pts',(-27.4555207700342,23.0840240612928,28.9943455659493));
#61535=CARTESIAN_POINT('Ctrl Pts',(-27.4372344644271,22.9308525305571,29.0021819269888));
#61536=CARTESIAN_POINT('Ctrl Pts',(-27.4099608272759,22.778993144504,29.0100182880282));
#61537=CARTESIAN_POINT('Ctrl Pts',(-27.3739131308343,22.6293244006311,29.0178546490677));
#61538=CARTESIAN_POINT('Ctrl Pts',(-27.34689356463,22.5171401299844,29.0237283968188));
#61539=CARTESIAN_POINT('Ctrl Pts',(-27.3148874883134,22.4059583868975,29.0296021445699));
#61540=CARTESIAN_POINT('Ctrl Pts',(-27.2779840235745,22.2962561503422,29.035475892321));
#61541=CARTESIAN_POINT('Ctrl Pts',(-27.2411284068907,22.1866961508015,29.0413420243263));
#61542=CARTESIAN_POINT('Ctrl Pts',(-27.1993881599582,22.0786122309629,29.0472081563316));
#61543=CARTESIAN_POINT('Ctrl Pts',(-27.1529031639015,21.9724700935057,29.0530742883369));
#61544=CARTESIAN_POINT('Ctrl Pts',(-27.106466020728,21.8664372215693,29.058934381591));
#61545=CARTESIAN_POINT('Ctrl Pts',(-27.0552940085456,21.7623425322087,29.064794474845));
#61546=CARTESIAN_POINT('Ctrl Pts',(-26.9995762403214,21.6606348579035,29.070654568099));
#61547=CARTESIAN_POINT('Ctrl Pts',(-26.9417014418957,21.5549897228528,29.0767415261133));
#61548=CARTESIAN_POINT('Ctrl Pts',(-26.8789219544355,21.4519205880235,29.0828284841276));
#61549=CARTESIAN_POINT('Ctrl Pts',(-26.8115041026131,21.3519060641921,29.088915442142));
#61550=CARTESIAN_POINT('Ctrl Pts',(-26.7466744075751,21.25573107635,29.0947687231515));
#61551=CARTESIAN_POINT('Ctrl Pts',(-26.677556166298,21.1623808660154,29.1006220041611));
#61552=CARTESIAN_POINT('Ctrl Pts',(-26.6044316819318,21.072253597422,29.1064752851707));
#61553=CARTESIAN_POINT('Ctrl Pts',(-26.5313184814589,20.9821402364343,29.1123276629561));
#61554=CARTESIAN_POINT('Ctrl Pts',(-26.4542005273581,20.8952491490648,29.1181800407415));
#61555=CARTESIAN_POINT('Ctrl Pts',(-26.3734010795189,20.8119462528212,29.1240324185269));
#61556=CARTESIAN_POINT('Ctrl Pts',(-26.2925945571716,20.7286360628765,29.1298853087254));
#61557=CARTESIAN_POINT('Ctrl Pts',(-26.2081061879956,20.6489149851832,29.1357381989239));
#61558=CARTESIAN_POINT('Ctrl Pts',(-26.1202963266871,20.5731123113118,29.1415910891225));
#61559=CARTESIAN_POINT('Ctrl Pts',(-26.0324575387834,20.4972846662899,29.1474459073981));
#61560=CARTESIAN_POINT('Ctrl Pts',(-25.9412953956253,20.4253782616515,29.1533007256738));
#61561=CARTESIAN_POINT('Ctrl Pts',(-25.8472030073224,20.3576818570636,29.1591555439494));
#61562=CARTESIAN_POINT('Ctrl Pts',(-25.7530041086937,20.2899088217701,29.1650169897388));
#61563=CARTESIAN_POINT('Ctrl Pts',(-25.6558686799156,20.226355540039,29.1708784355283));
#61564=CARTESIAN_POINT('Ctrl Pts',(-25.5562185432465,20.1672672582269,29.1767398813177));
#61565=CARTESIAN_POINT('Ctrl Pts',(-25.4565015736801,20.1081393473565,29.1826052582348));
#61566=CARTESIAN_POINT('Ctrl Pts',(-25.3542669013857,20.0534825936248,29.1884706351519));
#61567=CARTESIAN_POINT('Ctrl Pts',(-25.2499590890195,20.0034953340578,29.1943360120689));
#61568=CARTESIAN_POINT('Ctrl Pts',(-25.1454981624262,19.9534346978143,29.2002099988172));
#61569=CARTESIAN_POINT('Ctrl Pts',(-25.0389584008463,19.9080573971475,29.2060839855654));
#61570=CARTESIAN_POINT('Ctrl Pts',(-24.9308024499856,19.8675129368945,29.2119579723136));
#61571=CARTESIAN_POINT('Ctrl Pts',(-24.9014428602792,19.856506896927,29.2135525016899));
#61572=CARTESIAN_POINT('Ctrl Pts',(-24.8719642487308,19.8458566934534,29.2151470310662));
#61573=CARTESIAN_POINT('Ctrl Pts',(-24.8423760146667,19.835564670682,29.2167415604425));
#61574=CARTESIAN_POINT('Ctrl Pts',(-24.7333753579618,19.7976496927734,29.2226156774572));
#61575=CARTESIAN_POINT('Ctrl Pts',(-24.6225228972636,19.7644732561446,29.228489794472));
#61576=CARTESIAN_POINT('Ctrl Pts',(-24.5102682538304,19.7362180780937,29.2343639114867));
#61577=CARTESIAN_POINT('Ctrl Pts',(-24.3981586609349,19.7079994101474,29.2402304382245));
#61578=CARTESIAN_POINT('Ctrl Pts',(-24.2846508853829,19.6846894546324,29.2460969649623));
#61579=CARTESIAN_POINT('Ctrl Pts',(-24.1702124777709,19.6664221201983,29.2519634917001));
#61580=CARTESIAN_POINT('Ctrl Pts',(-24.0558913871888,19.6481735126013,29.2578240043426));
#61581=CARTESIAN_POINT('Ctrl Pts',(-23.9406419677007,19.6349573083073,29.2636845169851));
#61582=CARTESIAN_POINT('Ctrl Pts',(-23.8249441676021,19.6268568716617,29.2695450296275));
#61583=CARTESIAN_POINT('Ctrl Pts',(-23.7047788202789,19.6184436452894,29.2756318397188));
#61584=CARTESIAN_POINT('Ctrl Pts',(-23.584130207103,19.6155493418606,29.28171864981));
#61585=CARTESIAN_POINT('Ctrl Pts',(-23.4635448920503,19.6182084341252,29.2878054599013));
#61586=CARTESIAN_POINT('Ctrl Pts',(-23.3475765420952,19.6207657151852,29.2936592184826));
#61587=CARTESIAN_POINT('Ctrl Pts',(-23.2316671832364,19.6284589440699,29.2995129770639));
#61588=CARTESIAN_POINT('Ctrl Pts',(-23.1163044713861,19.6412656960864,29.3053667356452));
#61589=CARTESIAN_POINT('Ctrl Pts',(-23.000959155594,19.6540705169156,29.3112196115122));
#61590=CARTESIAN_POINT('Ctrl Pts',(-22.8861607333545,19.6719872821083,29.3170724873791));
#61591=CARTESIAN_POINT('Ctrl Pts',(-22.7723918519182,19.6949416800431,29.3229253632461));
#61592=CARTESIAN_POINT('Ctrl Pts',(-22.6586126238183,19.7178981655562,29.3287787714004));
#61593=CARTESIAN_POINT('Ctrl Pts',(-22.5458635275998,19.7458931128794,29.3346321795547));
#61594=CARTESIAN_POINT('Ctrl Pts',(-22.4346164315061,19.7788012073421,29.340485587709));
#61595=CARTESIAN_POINT('Ctrl Pts',(-22.3233323253789,19.8117202497731,29.3463409431935));
#61596=CARTESIAN_POINT('Ctrl Pts',(-22.2135516088998,19.8495555724328,29.352196298678));
#61597=CARTESIAN_POINT('Ctrl Pts',(-22.1057297411984,19.8921323986561,29.3580516541626));
#61598=CARTESIAN_POINT('Ctrl Pts',(-21.9977853623585,19.9347576022223,29.3639136627155));
#61599=CARTESIAN_POINT('Ctrl Pts',(-21.8918046592129,19.9821349108153,29.3697756712685));
#61600=CARTESIAN_POINT('Ctrl Pts',(-21.7882219911841,20.0340418761291,29.3756376798215));
#61601=CARTESIAN_POINT('Ctrl Pts',(-21.6845695848194,20.085983788461,29.3815036350456));
#61602=CARTESIAN_POINT('Ctrl Pts',(-21.583318788317,20.1424612293499,29.3873695902696));
#61603=CARTESIAN_POINT('Ctrl Pts',(-21.4848767760092,20.2032072694026,29.3932355454937));
#61604=CARTESIAN_POINT('Ctrl Pts',(-21.3862899701283,20.2640426578543,29.3991101286663));
#61605=CARTESIAN_POINT('Ctrl Pts',(-21.2905205340972,20.3291589447689,29.4049847118389));
#61606=CARTESIAN_POINT('Ctrl Pts',(-21.1979443244108,20.3982475986481,29.4108592950115));
#61607=CARTESIAN_POINT('Ctrl Pts',(-21.1728922030347,20.4169437339571,29.4124490206135));
#61608=CARTESIAN_POINT('Ctrl Pts',(-21.1480737204606,20.4359305512005,29.4140387462155));
#61609=CARTESIAN_POINT('Ctrl Pts',(-21.1234958640683,20.4552014697353,29.4156284718175));
#61610=CARTESIAN_POINT('Ctrl Pts',(-21.0328446115116,20.5262789825668,29.4214919049315));
#61611=CARTESIAN_POINT('Ctrl Pts',(-20.9451640888828,20.601463754417,29.4273553380455));
#61612=CARTESIAN_POINT('Ctrl Pts',(-20.8608504638897,20.6804780601218,29.4332187711595));
#61613=CARTESIAN_POINT('Ctrl Pts',(-20.7766465412602,20.7593895585271,29.4390745752282));
#61614=CARTESIAN_POINT('Ctrl Pts',(-20.6958011049263,20.8421204017871,29.4449303792968));
#61615=CARTESIAN_POINT('Ctrl Pts',(-20.6186790592074,20.9283513178015,29.4507861833654));
#61616=CARTESIAN_POINT('Ctrl Pts',(-20.5416365654878,21.014493285945,29.4566359471259));
#61617=CARTESIAN_POINT('Ctrl Pts',(-20.4683100983462,21.1041278389244,29.4624857108863));
#61618=CARTESIAN_POINT('Ctrl Pts',(-20.399028822363,21.1968978763673,29.4683354746468));
#61619=CARTESIAN_POINT('Ctrl Pts',(-20.326892500554,21.2934909194404,29.4744263041695));
#61620=CARTESIAN_POINT('Ctrl Pts',(-20.2591422635406,21.3934831060891,29.4805171336923));
#61621=CARTESIAN_POINT('Ctrl Pts',(-20.1961045467497,21.4964316302783,29.486607963215));
#61622=CARTESIAN_POINT('Ctrl Pts',(-20.1356316620657,21.5951914608784,29.4924509735604));
#61623=CARTESIAN_POINT('Ctrl Pts',(-20.0794955649851,21.6966713802769,29.4982939839058));
#61624=CARTESIAN_POINT('Ctrl Pts',(-20.0279405678685,21.8004504201712,29.5041369942511));
#61625=CARTESIAN_POINT('Ctrl Pts',(-19.9763932007642,21.9042141010238,29.5099791398454));
#61626=CARTESIAN_POINT('Ctrl Pts',(-19.9294257701819,22.0102758545438,29.5158212854397));
#61627=CARTESIAN_POINT('Ctrl Pts',(-19.8872362410366,22.1181908520249,29.5216634310339));
#61628=CARTESIAN_POINT('Ctrl Pts',(-19.8450426584752,22.2261162175855,29.5275061379203));
#61629=CARTESIAN_POINT('Ctrl Pts',(-19.8076280409059,22.3358947947495,29.5333488448066));
#61630=CARTESIAN_POINT('Ctrl Pts',(-19.7751416191933,22.447063246795,29.5391915516929));
#61631=CARTESIAN_POINT('Ctrl Pts',(-19.7426441471454,22.5582695130593,29.5450362459901));
#61632=CARTESIAN_POINT('Ctrl Pts',(-19.7150783203228,22.6708661963421,29.5508809402874));
#61633=CARTESIAN_POINT('Ctrl Pts',(-19.6925428826197,22.7843770434866,29.5567256345846));
#61634=CARTESIAN_POINT('Ctrl Pts',(-19.6699813573313,22.8980192936209,29.5625770948459));
#61635=CARTESIAN_POINT('Ctrl Pts',(-19.6524619248555,23.0125774127814,29.5684285551071));
#61636=CARTESIAN_POINT('Ctrl Pts',(-19.6400318126782,23.1275671539273,29.5742800153683));
#61637=CARTESIAN_POINT('Ctrl Pts',(-19.6275932055195,23.2426354813074,29.5801354746318));
#61638=CARTESIAN_POINT('Ctrl Pts',(-19.6202508698198,23.3581356051378,29.5859909338952));
#61639=CARTESIAN_POINT('Ctrl Pts',(-19.6179999132308,23.4735821685314,29.5918463931586));
#61640=CARTESIAN_POINT('Ctrl Pts',(-19.6157455789338,23.5892019670618,29.5977106389226));
#61641=CARTESIAN_POINT('Ctrl Pts',(-19.6185978609437,23.7047676317724,29.6035748846865));
#61642=CARTESIAN_POINT('Ctrl Pts',(-19.6264999418224,23.8197977291557,29.6094391304504));
#61643=CARTESIAN_POINT('Ctrl Pts',(-19.6287800281479,23.8529888032655,29.6111312146977));
#61644=CARTESIAN_POINT('Ctrl Pts',(-19.6314802181483,23.886135348282,29.612823298945));
#61645=CARTESIAN_POINT('Ctrl Pts',(-19.6345983585675,23.9192259676965,29.6145153831924));
#61646=CARTESIAN_POINT('Ctrl Pts',(-19.6454412758116,24.0342941813218,29.6203993803821));
#61647=CARTESIAN_POINT('Ctrl Pts',(-19.6613785537232,24.1490735677679,29.6262833775718));
#61648=CARTESIAN_POINT('Ctrl Pts',(-19.6823889312802,24.2630780142579,29.6321673747616));
#61649=CARTESIAN_POINT('Ctrl Pts',(-19.7033720247706,24.3769344146267,29.6380437309953));
#61650=CARTESIAN_POINT('Ctrl Pts',(-19.7294150418344,24.4900174753028,29.643920087229));
#61651=CARTESIAN_POINT('Ctrl Pts',(-19.7604448812621,24.6018451204501,29.6497964434627));
#61652=CARTESIAN_POINT('Ctrl Pts',(-19.7914426384536,24.7135571452464,29.6556667240398));
#61653=CARTESIAN_POINT('Ctrl Pts',(-19.8274168522906,24.8240159422113,29.661537004617));
#61654=CARTESIAN_POINT('Ctrl Pts',(-19.8682433048668,24.9327492056714,29.6674072851941));
#61655=CARTESIAN_POINT('Ctrl Pts',(-19.9105500442143,25.0454249231371,29.6734904105846));
#61656=CARTESIAN_POINT('Ctrl Pts',(-19.9580674810231,25.1562471619692,29.6795735359752));
#61657=CARTESIAN_POINT('Ctrl Pts',(-20.0106005710162,25.2647066714332,29.6856566613657));
#61658=CARTESIAN_POINT('Ctrl Pts',(-20.0612353894315,25.3692470205321,29.6915199743669));
#61659=CARTESIAN_POINT('Ctrl Pts',(-20.1165294634138,25.471592034314,29.6973832873681));
#61660=CARTESIAN_POINT('Ctrl Pts',(-20.1762592759672,25.5713063435232,29.7032466003692));
#61661=CARTESIAN_POINT('Ctrl Pts',(-20.2359791282306,25.6710040247975,29.7091089356292));
#61662=CARTESIAN_POINT('Ctrl Pts',(-20.3001330366619,25.7680715208699,29.7149712708892));
#61663=CARTESIAN_POINT('Ctrl Pts',(-20.3684523581246,25.8620995542008,29.7208336061492));
#61664=CARTESIAN_POINT('Ctrl Pts',(-20.436776660008,25.9561344420957,29.7266963687684));
#61665=CARTESIAN_POINT('Ctrl Pts',(-20.5092667365253,26.0471290938087,29.7325591313877));
#61666=CARTESIAN_POINT('Ctrl Pts',(-20.5856120051761,26.1347051910645,29.738421894007));
#61667=CARTESIAN_POINT('Ctrl Pts',(-20.6619811356613,26.222308660368,29.7442864890419));
#61668=CARTESIAN_POINT('Ctrl Pts',(-20.7422075839998,26.3064911403823,29.7501510840769));
#61669=CARTESIAN_POINT('Ctrl Pts',(-20.8259425513158,26.3869097423579,29.7560156791119));
#61670=CARTESIAN_POINT('Ctrl Pts',(-20.909769426386,26.4674166120351,29.7618867111442));
#61671=CARTESIAN_POINT('Ctrl Pts',(-20.9971122099963,26.5441510722723,29.7677577431765));
#61672=CARTESIAN_POINT('Ctrl Pts',(-21.0875874616023,26.6168091922745,29.7736287752088));
#61673=CARTESIAN_POINT('Ctrl Pts',(-21.1781217604102,26.6895147314173,29.7795036388746));
#61674=CARTESIAN_POINT('Ctrl Pts',(-21.2717922672247,26.7581383894613,29.7853785025405));
#61675=CARTESIAN_POINT('Ctrl Pts',(-21.3681862871104,26.8224193832236,29.7912533662064));
#61676=CARTESIAN_POINT('Ctrl Pts',(-21.4647179948349,26.8867921950377,29.7971366214435));
#61677=CARTESIAN_POINT('Ctrl Pts',(-21.5639806290897,26.9468097497583,29.8030198766806));
#61678=CARTESIAN_POINT('Ctrl Pts',(-21.6655365762954,27.0022569881608,29.8089031319177));
#61679=CARTESIAN_POINT('Ctrl Pts',(-21.6914245530531,27.0163912349335,29.8104028528009));
#61680=CARTESIAN_POINT('Ctrl Pts',(-21.7174614503872,27.0302287427097,29.8119025736841));
#61681=CARTESIAN_POINT('Ctrl Pts',(-21.7436398252607,27.0437664545165,29.8134022945673));
#61682=CARTESIAN_POINT('Ctrl Pts',(-21.8453103654917,27.096343685897,29.8192268514058));
#61683=CARTESIAN_POINT('Ctrl Pts',(-21.9494591145075,27.144572387477,29.8250514082443));
#61684=CARTESIAN_POINT('Ctrl Pts',(-22.0556742954077,27.1882086743131,29.8308759650828));
#61685=CARTESIAN_POINT('Ctrl Pts',(-22.1617537537081,27.2317892023562,29.8366930792565));
#61686=CARTESIAN_POINT('Ctrl Pts',(-22.2698940091309,27.2707888232274,29.8425101934301));
#61687=CARTESIAN_POINT('Ctrl Pts',(-22.379658318945,27.3050092733591,29.8483273076037));
#61688=CARTESIAN_POINT('Ctrl Pts',(-22.4893129316497,27.3391955239913,29.8541386082246));
#61689=CARTESIAN_POINT('Ctrl Pts',(-22.6005879721008,27.3686119767023,29.8599499088454));
#61690=CARTESIAN_POINT('Ctrl Pts',(-22.7130270413074,27.3931085631175,29.8657612094662));
#61691=CARTESIAN_POINT('Ctrl Pts',(-22.825387957362,27.4175881226625,29.8715684708197));
#61692=CARTESIAN_POINT('Ctrl Pts',(-22.9389108834846,27.43715452698,29.8773757321732));
#61693=CARTESIAN_POINT('Ctrl Pts',(-23.0531252998253,27.4517078390551,29.8831829935267));
#61694=CARTESIAN_POINT('Ctrl Pts',(-23.1672987307487,27.4662559287284,29.8889881709661));
#61695=CARTESIAN_POINT('Ctrl Pts',(-23.2821627419183,27.4757944482306,29.8947933484056));
#61696=CARTESIAN_POINT('Ctrl Pts',(-23.3972383674406,27.4802748809357,29.900598525845));
#61697=CARTESIAN_POINT('Ctrl Pts',(-23.5123016844848,27.4847548344141,29.9064030823632));
#61698=CARTESIAN_POINT('Ctrl Pts',(-23.6275761505149,27.4841777605835,29.9122076388813));
#61699=CARTESIAN_POINT('Ctrl Pts',(-23.7425802607441,27.4785472055493,29.9180121953995));
#61700=CARTESIAN_POINT('Ctrl Pts',(-23.8576010389199,27.4729158344591,29.9238175931923));
#61701=CARTESIAN_POINT('Ctrl Pts',(-23.9723509632556,27.4622295477953,29.9296229909851));
#61702=CARTESIAN_POINT('Ctrl Pts',(-24.0863519321435,27.4465439007833,29.9354283887779));
#61703=CARTESIAN_POINT('Ctrl Pts',(-24.2004654002933,27.4308427747474,29.9412395154954));
#61704=CARTESIAN_POINT('Ctrl Pts',(-24.3138280197813,27.4101324947749,29.9470506422129));
#61705=CARTESIAN_POINT('Ctrl Pts',(-24.4259701600802,27.3845200804359,29.9528617689304));
#61706=CARTESIAN_POINT('Ctrl Pts',(-24.5381711727251,27.3588942200997,29.9586759463714));
#61707=CARTESIAN_POINT('Ctrl Pts',(-24.6491500250568,27.328361212771,29.9644901238124));
#61708=CARTESIAN_POINT('Ctrl Pts',(-24.7584523537206,27.2930779604385,29.9703043012534));
#61709=CARTESIAN_POINT('Ctrl Pts',(-24.8679220240612,27.2577406895076,29.97612738019));
#61710=CARTESIAN_POINT('Ctrl Pts',(-24.9757096508579,27.2176387965406,29.9819504591267));
#61711=CARTESIAN_POINT('Ctrl Pts',(-25.0813807158189,27.1729774017028,29.9877735380633));
#61712=CARTESIAN_POINT('Ctrl Pts',(-25.1549762723192,27.1418725745831,29.9918290733704));
#61713=CARTESIAN_POINT('Ctrl Pts',(-25.2275456364601,27.1085571364939,29.9958846086775));
#61714=CARTESIAN_POINT('Ctrl Pts',(-25.2989497345943,27.0731131722205,29.9999401439846));
#61715=CARTESIAN_POINT('',(-21.801558056363,27.073114526145,30.));
#61716=CARTESIAN_POINT('Origin',(-23.5502525316942,23.5502525316942,30.));
#61717=CARTESIAN_POINT('',(-27.4823597385963,23.5463452821269,29.1541635220348));
#61718=CARTESIAN_POINT('Ctrl Pts',(-21.801558056363,27.073114526145,30.));
#61719=CARTESIAN_POINT('Ctrl Pts',(-20.6276058013427,26.4903826945007,29.933704362875));
#61720=CARTESIAN_POINT('Ctrl Pts',(-18.9286240350797,24.0691044546063,29.8011130886252));
#61721=CARTESIAN_POINT('Ctrl Pts',(-20.6189893842979,19.933885741136,29.6022261772502));
#61722=CARTESIAN_POINT('Ctrl Pts',(-25.0066490640735,19.1336642374115,29.4033392658754));
#61723=CARTESIAN_POINT('Ctrl Pts',(-27.2951287691289,21.5759483018016,29.2539850474702));
#61724=CARTESIAN_POINT('Ctrl Pts',(-27.4853611242349,23.2148653571988,29.17092646619));
#61725=CARTESIAN_POINT('Ctrl Pts',(-27.4823597385963,23.5463452821269,29.1541635220348));
#61726=CARTESIAN_POINT('',(-27.4808119672486,23.5510682671432,27.9041634967419));
#61727=CARTESIAN_POINT('Ctrl Pts',(-27.4823597385963,23.5463452821269,29.1541635220348));
#61728=CARTESIAN_POINT('Ctrl Pts',(-27.4734909675771,24.5258327274734,29.104630829065));
#61729=CARTESIAN_POINT('Ctrl Pts',(-26.6075785985611,26.8308346334369,28.9888024989704));
#61730=CARTESIAN_POINT('Ctrl Pts',(-22.7363170503599,28.1302192147636,28.8066785317506));
#61731=CARTESIAN_POINT('Ctrl Pts',(-19.256958269279,25.3414769801662,28.6077916203758));
#61732=CARTESIAN_POINT('Ctrl Pts',(-19.7226238927422,20.9062869097954,28.4089047090008));
#61733=CARTESIAN_POINT('Ctrl Pts',(-23.7056346214918,18.9009230350342,28.2100177976262));
#61734=CARTESIAN_POINT('Ctrl Pts',(-26.9542144477632,20.8185459147253,28.0417707353038));
#61735=CARTESIAN_POINT('Ctrl Pts',(-27.4755714141968,22.8435015405095,27.9398193101068));
#61736=CARTESIAN_POINT('Ctrl Pts',(-27.476881774362,23.5510669492537,27.9041635220347));
#61737=CARTESIAN_POINT('',(-27.4835625131296,23.5535968072644,26.6541635220347));
#61738=CARTESIAN_POINT('Ctrl Pts',(-27.4832524469294,23.5510690854955,27.9041634810362));
#61739=CARTESIAN_POINT('Ctrl Pts',(-27.483226718146,23.674993930109,27.8979287463526));
#61740=CARTESIAN_POINT('Ctrl Pts',(-27.4773396257473,23.798767939476,27.8916940116689));
#61741=CARTESIAN_POINT('Ctrl Pts',(-27.4656591995897,23.9218432003061,27.8854592769853));
#61742=CARTESIAN_POINT('Ctrl Pts',(-27.4539388249783,24.0453393932415,27.8792032187637));
#61743=CARTESIAN_POINT('Ctrl Pts',(-27.4363855054114,24.1681317315402,27.8729471605421));
#61744=CARTESIAN_POINT('Ctrl Pts',(-27.4131189223168,24.289679504558,27.8666911023205));
#61745=CARTESIAN_POINT('Ctrl Pts',(-27.3898124520038,24.4114356537924,27.8604243189847));
#61746=CARTESIAN_POINT('Ctrl Pts',(-27.3607732399586,24.5319426631247,27.854157535649));
#61747=CARTESIAN_POINT('Ctrl Pts',(-27.3261710053763,24.6506745780502,27.8478907523132));
#61748=CARTESIAN_POINT('Ctrl Pts',(-27.2914641228452,24.7697655753152,27.8416050162702));
#61749=CARTESIAN_POINT('Ctrl Pts',(-27.2511606637123,24.8870704295725,27.8353192802272));
#61750=CARTESIAN_POINT('Ctrl Pts',(-27.2054795296194,25.0020805496216,27.8290335441842));
#61751=CARTESIAN_POINT('Ctrl Pts',(-27.1648072009441,25.1044801396603,27.8234370210816));
#61752=CARTESIAN_POINT('Ctrl Pts',(-27.1198725839544,25.2050608095957,27.8178404979789));
#61753=CARTESIAN_POINT('Ctrl Pts',(-27.0708602533607,25.3034810593374,27.8122439748763));
#61754=CARTESIAN_POINT('Ctrl Pts',(-27.0194322238423,25.4067522045293,27.8063716127209));
#61755=CARTESIAN_POINT('Ctrl Pts',(-26.9633702720088,25.5079315737953,27.8004992505656));
#61756=CARTESIAN_POINT('Ctrl Pts',(-26.9028678598677,25.6065743599341,27.7946268884102));
#61757=CARTESIAN_POINT('Ctrl Pts',(-26.8424438475145,25.7050893235079,27.7887621357357));
#61758=CARTESIAN_POINT('Ctrl Pts',(-26.7775910316421,25.8010738913747,27.7828973830612));
#61759=CARTESIAN_POINT('Ctrl Pts',(-26.7085498266344,25.894105598073,27.7770326303867));
#61760=CARTESIAN_POINT('Ctrl Pts',(-26.6395796198831,25.9870416359751,27.771173908708));
#61761=CARTESIAN_POINT('Ctrl Pts',(-26.5664298359389,26.0770305226398,27.7653151870293));
#61762=CARTESIAN_POINT('Ctrl Pts',(-26.4893851003473,26.1636772472509,27.7594564653505));
#61763=CARTESIAN_POINT('Ctrl Pts',(-26.4093321581784,26.2537070874619,27.7533689902735));
#61764=CARTESIAN_POINT('Ctrl Pts',(-26.3250741477172,26.3401280706287,27.7472815151964));
#61765=CARTESIAN_POINT('Ctrl Pts',(-26.2369779545704,26.4225330719741,27.7411940401194));
#61766=CARTESIAN_POINT('Ctrl Pts',(-26.1522904003884,26.5017496393084,27.7353421030832));
#61767=CARTESIAN_POINT('Ctrl Pts',(-26.0640564887503,26.5772549144733,27.7294901660471));
#61768=CARTESIAN_POINT('Ctrl Pts',(-25.9726403486848,26.6487241329995,27.7236382290109));
#61769=CARTESIAN_POINT('Ctrl Pts',(-25.8812381248608,26.7201824717959,27.7177871828128));
#61770=CARTESIAN_POINT('Ctrl Pts',(-25.7866549613817,26.787605721061,27.7119361366146));
#61771=CARTESIAN_POINT('Ctrl Pts',(-25.6892876858399,26.8507097135599,27.7060850904164));
#61772=CARTESIAN_POINT('Ctrl Pts',(-25.5919116546241,26.9138193806346,27.7002335180676));
#61773=CARTESIAN_POINT('Ctrl Pts',(-25.4917513605651,26.9726087939943,27.6943819457188));
#61774=CARTESIAN_POINT('Ctrl Pts',(-25.3892315831579,27.026837788563,27.68853037337));
#61775=CARTESIAN_POINT('Ctrl Pts',(-25.2866777612029,27.08108479138,27.6826768578436));
#61776=CARTESIAN_POINT('Ctrl Pts',(-25.1817632631024,27.1307681709063,27.6768233423172));
#61777=CARTESIAN_POINT('Ctrl Pts',(-25.0749357138907,27.1756946004532,27.6709698267908));
#61778=CARTESIAN_POINT('Ctrl Pts',(-24.967986685618,27.2206721181371,27.6651096549331));
#61779=CARTESIAN_POINT('Ctrl Pts',(-24.8591206454175,27.2608817285548,27.6592494830753));
#61780=CARTESIAN_POINT('Ctrl Pts',(-24.7488034557539,27.2961789434695,27.6533893112175));
#61781=CARTESIAN_POINT('Ctrl Pts',(-24.6384119770577,27.3314999279885,27.6475251930436));
#61782=CARTESIAN_POINT('Ctrl Pts',(-24.5265678009756,27.3619018218082,27.6416610748698));
#61783=CARTESIAN_POINT('Ctrl Pts',(-24.4137484405707,27.3872909489313,27.6357969566959));
#61784=CARTESIAN_POINT('Ctrl Pts',(-24.3007628216028,27.4127174912621,27.6299241967441));
#61785=CARTESIAN_POINT('Ctrl Pts',(-24.1867995555143,27.4331164509735,27.6240514367923));
#61786=CARTESIAN_POINT('Ctrl Pts',(-24.0723428370296,27.4484457943577,27.6181786768405));
#61787=CARTESIAN_POINT('Ctrl Pts',(-24.0410193454553,27.4526409920244,27.6165714723941));
#61788=CARTESIAN_POINT('Ctrl Pts',(-24.0096589026459,27.4564567976675,27.6149642679477));
#61789=CARTESIAN_POINT('Ctrl Pts',(-23.9782714292153,27.4598930296639,27.6133570635013));
#61790=CARTESIAN_POINT('Ctrl Pts',(-23.8635896720581,27.47244813781,27.6074847517197));
#61791=CARTESIAN_POINT('Ctrl Pts',(-23.7481629177312,27.4799740475433,27.601612439938));
#61792=CARTESIAN_POINT('Ctrl Pts',(-23.6324699563696,27.4823930804386,27.5957401281563));
#61793=CARTESIAN_POINT('Ctrl Pts',(-23.5169269156114,27.4848089786326,27.5898754260038));
#61794=CARTESIAN_POINT('Ctrl Pts',(-23.4011187633041,27.4821311517403,27.5840107238512));
#61795=CARTESIAN_POINT('Ctrl Pts',(-23.2855308734857,27.4743334997268,27.5781460216987));
#61796=CARTESIAN_POINT('Ctrl Pts',(-23.170061850753,27.4665438665825,27.5722873506282));
#61797=CARTESIAN_POINT('Ctrl Pts',(-23.0548130499301,27.4536449084763,27.5664286795578));
#61798=CARTESIAN_POINT('Ctrl Pts',(-22.9402706455418,27.4356625613521,27.5605700084873));
#61799=CARTESIAN_POINT('Ctrl Pts',(-22.8212545422657,27.416977875153,27.5544825144723));
#61800=CARTESIAN_POINT('Ctrl Pts',(-22.7030015944435,27.3928046108824,27.5483950204572));
#61801=CARTESIAN_POINT('Ctrl Pts',(-22.5860526519863,27.3632313661452,27.5423075264422));
#61802=CARTESIAN_POINT('Ctrl Pts',(-22.473630045844,27.3348027102241,27.5364556399038));
#61803=CARTESIAN_POINT('Ctrl Pts',(-22.3624128206967,27.3013844096332,27.5306037533654));
#61804=CARTESIAN_POINT('Ctrl Pts',(-22.2528710272477,27.2631072597869,27.524751866827));
#61805=CARTESIAN_POINT('Ctrl Pts',(-22.1433459070482,27.2248359360682,27.5189008709985));
#61806=CARTESIAN_POINT('Ctrl Pts',(-22.0354961016288,27.1817073699025,27.5130498751701));
#61807=CARTESIAN_POINT('Ctrl Pts',(-21.9297751816476,27.1339018111279,27.5071988793416));
#61808=CARTESIAN_POINT('Ctrl Pts',(-21.8240447514147,27.0860919519471,27.5013473571798));
#61809=CARTESIAN_POINT('Ctrl Pts',(-21.7204439640015,27.033604434127,27.495495835018));
#61810=CARTESIAN_POINT('Ctrl Pts',(-21.6194044795231,26.9766668089565,27.4896443128562));
#61811=CARTESIAN_POINT('Ctrl Pts',(-21.5183314376796,26.9197102735879,27.4837908472793));
#61812=CARTESIAN_POINT('Ctrl Pts',(-21.4198217502063,26.8583008948426,27.4779373817024));
#61813=CARTESIAN_POINT('Ctrl Pts',(-21.3242800202089,26.792710762437,27.4720839161254));
#61814=CARTESIAN_POINT('Ctrl Pts',(-21.2286296339778,26.7270460366914,27.4662237936089));
#61815=CARTESIAN_POINT('Ctrl Pts',(-21.1359542833283,26.6571913013016,27.4603636710924));
#61816=CARTESIAN_POINT('Ctrl Pts',(-21.0466273407646,26.5834603886243,27.4545035485759));
#61817=CARTESIAN_POINT('Ctrl Pts',(-20.957240239299,26.5096798204835,27.4486394794501));
#61818=CARTESIAN_POINT('Ctrl Pts',(-20.8712063422712,26.4320181533777,27.4427754103244));
#61819=CARTESIAN_POINT('Ctrl Pts',(-20.7888625704094,26.3508264874604,27.4369113411986));
#61820=CARTESIAN_POINT('Ctrl Pts',(-20.7063974385128,26.2695151595069,27.4310386294808));
#61821=CARTESIAN_POINT('Ctrl Pts',(-20.6276335663296,26.1846637512108,27.4251659177629));
#61822=CARTESIAN_POINT('Ctrl Pts',(-20.5528680385805,26.0966568987265,27.4192932060451));
#61823=CARTESIAN_POINT('Ctrl Pts',(-20.5324005958888,26.0725645761826,27.4176855214055));
#61824=CARTESIAN_POINT('Ctrl Pts',(-20.512232546352,26.0482359470459,27.416077836766));
#61825=CARTESIAN_POINT('Ctrl Pts',(-20.4923694101848,26.0236792670531,27.4144701521264));
#61826=CARTESIAN_POINT('Ctrl Pts',(-20.4198168088736,25.9339829070196,27.4085978819217));
#61827=CARTESIAN_POINT('Ctrl Pts',(-20.3510925689731,25.8409413013264,27.402725611717));
#61828=CARTESIAN_POINT('Ctrl Pts',(-20.2865208506764,25.7449152653097,27.3968533415123));
#61829=CARTESIAN_POINT('Ctrl Pts',(-20.2220328168015,25.6490136782547,27.390988681722));
#61830=CARTESIAN_POINT('Ctrl Pts',(-20.16168683094,25.5501356924103,27.3851240219316));
#61831=CARTESIAN_POINT('Ctrl Pts',(-20.1057672190686,25.4486755433296,27.3792593621413));
#61832=CARTESIAN_POINT('Ctrl Pts',(-20.0499051206154,25.3473197461889,27.3734007341638));
#61833=CARTESIAN_POINT('Ctrl Pts',(-19.9984605392699,25.2433874281164,27.3675421061864));
#61834=CARTESIAN_POINT('Ctrl Pts',(-19.9516744554885,25.1373016265402,27.3616834782089));
#61835=CARTESIAN_POINT('Ctrl Pts',(-19.9030605566341,25.0270713184896,27.3555959683148));
#61836=CARTESIAN_POINT('Ctrl Pts',(-19.8594768223093,24.9145162110629,27.3495084584207));
#61837=CARTESIAN_POINT('Ctrl Pts',(-19.8211410761401,24.800139227381,27.3434209485267));
#61838=CARTESIAN_POINT('Ctrl Pts',(-19.784289435815,24.6901901619447,27.3375691066426));
#61839=CARTESIAN_POINT('Ctrl Pts',(-19.7522871494092,24.5785580873333,27.3317172647585));
#61840=CARTESIAN_POINT('Ctrl Pts',(-19.7252782618679,24.4657091582838,27.3258654228744));
#61841=CARTESIAN_POINT('Ctrl Pts',(-19.698273487673,24.3528774156784,27.3200144722026));
#61842=CARTESIAN_POINT('Ctrl Pts',(-19.6762606964705,24.2388295890369,27.3141635215308));
#61843=CARTESIAN_POINT('Ctrl Pts',(-19.6593334183605,24.1240447009457,27.308312570859));
#61844=CARTESIAN_POINT('Ctrl Pts',(-19.6424046188457,24.0092494961179,27.3024610943104));
#61845=CARTESIAN_POINT('Ctrl Pts',(-19.6305623013696,23.8937175071375,27.2966096177617));
#61846=CARTESIAN_POINT('Ctrl Pts',(-19.6238483570215,23.7779348918206,27.2907581412131));
#61847=CARTESIAN_POINT('Ctrl Pts',(-19.6171321832835,23.6621138304607,27.2849047216601));
#61848=CARTESIAN_POINT('Ctrl Pts',(-19.6155477926907,23.5460423897593,27.2790513021072));
#61849=CARTESIAN_POINT('Ctrl Pts',(-19.6190849799541,23.4302080393346,27.2731978825542));
#61850=CARTESIAN_POINT('Ctrl Pts',(-19.6226261897369,23.3142419611053,27.267337806443));
#61851=CARTESIAN_POINT('Ctrl Pts',(-19.6313005898805,23.1985139247478,27.2614777303317));
#61852=CARTESIAN_POINT('Ctrl Pts',(-19.6450459748211,23.083507689028,27.2556176542204));
#61853=CARTESIAN_POINT('Ctrl Pts',(-19.6588006162657,22.9684240050817,27.2497536317797));
#61854=CARTESIAN_POINT('Ctrl Pts',(-19.6776329753126,22.8540634965506,27.2438896093389));
#61855=CARTESIAN_POINT('Ctrl Pts',(-19.7014297885899,22.7408993997651,27.2380255868981));
#61856=CARTESIAN_POINT('Ctrl Pts',(-19.7252616741966,22.6275685189475,27.2321529219167));
#61857=CARTESIAN_POINT('Ctrl Pts',(-19.754072514336,22.5154379679629,27.2262802569353));
#61858=CARTESIAN_POINT('Ctrl Pts',(-19.7876992981181,22.4049655962468,27.2204075919539));
#61859=CARTESIAN_POINT('Ctrl Pts',(-19.7969073501856,22.374714848588,27.2187994748864));
#61860=CARTESIAN_POINT('Ctrl Pts',(-19.8064762409999,22.3445883171907,27.217191357819));
#61861=CARTESIAN_POINT('Ctrl Pts',(-19.8164020055153,22.3145951163264,27.2155832407515));
#61862=CARTESIAN_POINT('Ctrl Pts',(-19.8526475929278,22.2050699324456,27.2097109326137));
#61863=CARTESIAN_POINT('Ctrl Pts',(-19.8937770450568,22.0969574122162,27.2038386244759));
#61864=CARTESIAN_POINT('Ctrl Pts',(-19.9396620167432,21.9907253170083,27.1979663163381));
#61865=CARTESIAN_POINT('Ctrl Pts',(-19.9854875261016,21.884630887957,27.1921016181236));
#61866=CARTESIAN_POINT('Ctrl Pts',(-20.0360561372611,21.7804124139129,27.186236919909));
#61867=CARTESIAN_POINT('Ctrl Pts',(-20.0911898562017,21.6785222073647,27.1803722216945));
#61868=CARTESIAN_POINT('Ctrl Pts',(-20.1462668745483,21.5767367866961,27.1745135548502));
#61869=CARTESIAN_POINT('Ctrl Pts',(-20.2058994668376,21.4772752322489,27.1686548880059));
#61870=CARTESIAN_POINT('Ctrl Pts',(-20.2698619777202,21.3805689572073,27.1627962211616));
#61871=CARTESIAN_POINT('Ctrl Pts',(-20.3363227454924,21.2800855146568,27.1567087256706));
#61872=CARTESIAN_POINT('Ctrl Pts',(-20.4074583835905,21.1825773885528,27.1506212301795));
#61873=CARTESIAN_POINT('Ctrl Pts',(-20.4829635182502,21.0884996789477,27.1445337346885));
#61874=CARTESIAN_POINT('Ctrl Pts',(-20.5555462593645,20.9980632063597,27.1386818530747));
#61875=CARTESIAN_POINT('Ctrl Pts',(-20.6321662640687,20.910796894421,27.1328299714609));
#61876=CARTESIAN_POINT('Ctrl Pts',(-20.7125092049126,20.8270739089618,27.1269780898471));
#61877=CARTESIAN_POINT('Ctrl Pts',(-20.7928399133843,20.7433636704933,27.121127099194));
#61878=CARTESIAN_POINT('Ctrl Pts',(-20.876892144824,20.6631959840297,27.1152761085408));
#61879=CARTESIAN_POINT('Ctrl Pts',(-20.9643134406852,20.5869084717525,27.1094251178876));
#61880=CARTESIAN_POINT('Ctrl Pts',(-21.0517425969594,20.5106141001473,27.1035736011474));
#61881=CARTESIAN_POINT('Ctrl Pts',(-21.1425411083622,20.4382008680885,27.0977220844073));
#61882=CARTESIAN_POINT('Ctrl Pts',(-21.2363226005084,20.3699668096933,27.0918705676671));
#61883=CARTESIAN_POINT('Ctrl Pts',(-21.3301352356322,20.3017100921177,27.0860171077541));
#61884=CARTESIAN_POINT('Ctrl Pts',(-21.4269324871336,20.2376355508792,27.080163647841));
#61885=CARTESIAN_POINT('Ctrl Pts',(-21.5262987168613,20.1779980995044,27.074310187928));
#61886=CARTESIAN_POINT('Ctrl Pts',(-21.6257779467384,20.1182928278961,27.0684500714089));
#61887=CARTESIAN_POINT('Ctrl Pts',(-21.7278316313432,20.0630349304664,27.0625899548898));
#61888=CARTESIAN_POINT('Ctrl Pts',(-21.8320191463023,20.0124335660991,27.0567298383707));
#61889=CARTESIAN_POINT('Ctrl Pts',(-21.9362768247783,19.961798125003,27.0508657754442));
#61890=CARTESIAN_POINT('Ctrl Pts',(-22.0426708164094,19.915825624682,27.0450017125176));
#61891=CARTESIAN_POINT('Ctrl Pts',(-22.1507417506603,19.8746765803949,27.0391376495911));
#61892=CARTESIAN_POINT('Ctrl Pts',(-22.2589719577502,19.8334668914474,27.0332649443228));
#61893=CARTESIAN_POINT('Ctrl Pts',(-22.3688836490108,19.7970949755413,27.0273922390545));
#61894=CARTESIAN_POINT('Ctrl Pts',(-22.4800035085378,19.7656711772465,27.0215195337862));
#61895=CARTESIAN_POINT('Ctrl Pts',(-22.5104241166434,19.7570684751087,27.019911798983));
#61896=CARTESIAN_POINT('Ctrl Pts',(-22.540935223925,19.7488363205333,27.0183040641798));
#61897=CARTESIAN_POINT('Ctrl Pts',(-22.5715270262102,19.7409763032073,27.0166963293766));
#61898=CARTESIAN_POINT('Ctrl Pts',(-22.6832644728893,19.7122673615547,27.0108240312959));
#61899=CARTESIAN_POINT('Ctrl Pts',(-22.7964533581284,19.6884308827569,27.0049517332151));
#61900=CARTESIAN_POINT('Ctrl Pts',(-22.9106307722246,19.6696117334738,26.9990794351344));
#61901=CARTESIAN_POINT('Ctrl Pts',(-23.0246602223877,19.6508169721606,26.9932147470379));
#61902=CARTESIAN_POINT('Ctrl Pts',(-23.1396752497509,19.6370266767862,26.9873500589414));
#61903=CARTESIAN_POINT('Ctrl Pts',(-23.2551991045552,19.6283355928576,26.9814853708449));
#61904=CARTESIAN_POINT('Ctrl Pts',(-23.3706041512106,19.6196534470968,26.975626714167));
#61905=CARTESIAN_POINT('Ctrl Pts',(-23.4865165747105,19.6160601126637,26.9697680574892));
#61906=CARTESIAN_POINT('Ctrl Pts',(-23.602451445135,19.6175989398512,26.9639094008114));
#61907=CARTESIAN_POINT('Ctrl Pts',(-23.722914800385,19.6191978745416,26.9578219015276));
#61908=CARTESIAN_POINT('Ctrl Pts',(-23.8434019432624,19.6263381487003,26.9517344022439));
#61909=CARTESIAN_POINT('Ctrl Pts',(-23.9633649206812,19.6390088478942,26.9456469029602));
#61910=CARTESIAN_POINT('Ctrl Pts',(-24.0786845097008,19.6511891042956,26.939795031569));
#61911=CARTESIAN_POINT('Ctrl Pts',(-24.1935193069066,19.6684795683318,26.9339431601778));
#61912=CARTESIAN_POINT('Ctrl Pts',(-24.3073854556428,19.6908175036787,26.9280912887866));
#61913=CARTESIAN_POINT('Ctrl Pts',(-24.4212342679388,19.7131520380124,26.9222403083593));
#61914=CARTESIAN_POINT('Ctrl Pts',(-24.5341143194623,19.7405324360917,26.9163893279319));
#61915=CARTESIAN_POINT('Ctrl Pts',(-24.645551045502,19.7728446684035,26.9105383475045));
#61916=CARTESIAN_POINT('Ctrl Pts',(-24.7569977914472,19.8051598060906,26.9046868409825));
#61917=CARTESIAN_POINT('Ctrl Pts',(-24.8670005568701,19.8424075444164,26.8988353344604));
#61918=CARTESIAN_POINT('Ctrl Pts',(-24.9750997501867,19.8844239208677,26.8929838279384));
#61919=CARTESIAN_POINT('Ctrl Pts',(-25.0832348415141,19.9264542502847,26.8871303782247));
#61920=CARTESIAN_POINT('Ctrl Pts',(-25.1894647186556,19.973256217012,26.881276928511));
#61921=CARTESIAN_POINT('Ctrl Pts',(-25.2933502497918,20.0246179299291,26.8754234787974));
#61922=CARTESIAN_POINT('Ctrl Pts',(-25.3973539220852,20.0760380526377,26.8695633723981));
#61923=CARTESIAN_POINT('Ctrl Pts',(-25.4990075562372,20.1320280882276,26.8637032659988));
#61924=CARTESIAN_POINT('Ctrl Pts',(-25.5978970084691,20.1923303919278,26.8578431595995));
#61925=CARTESIAN_POINT('Ctrl Pts',(-25.6968530570032,20.252673305727,26.8519791067589));
#61926=CARTESIAN_POINT('Ctrl Pts',(-25.7930408747363,20.3173340401402,26.8461150539183));
#61927=CARTESIAN_POINT('Ctrl Pts',(-25.8860771095247,20.3860128850171,26.8402510010777));
#61928=CARTESIAN_POINT('Ctrl Pts',(-25.9792504615759,20.4547929491152,26.8343783057671));
#61929=CARTESIAN_POINT('Ctrl Pts',(-26.069262640328,20.527602683669,26.8285056104564));
#61930=CARTESIAN_POINT('Ctrl Pts',(-26.1557649650478,20.604103526698,26.8226329151457));
#61931=CARTESIAN_POINT('Ctrl Pts',(-26.1794476578128,20.6250480038273,26.8210250827644));
#61932=CARTESIAN_POINT('Ctrl Pts',(-26.2028674896014,20.6462689497625,26.8194172503831));
#61933=CARTESIAN_POINT('Ctrl Pts',(-26.2260178222051,20.667758974009,26.8178094180017));
#61934=CARTESIAN_POINT('Ctrl Pts',(-26.3093104344281,20.7450779606023,26.8120245957553));
#61935=CARTESIAN_POINT('Ctrl Pts',(-26.3894084840011,20.8261585613254,26.8062397735089));
#61936=CARTESIAN_POINT('Ctrl Pts',(-26.4659450914145,20.9107022106752,26.8004549512625));
#61937=CARTESIAN_POINT('Ctrl Pts',(-26.5423814324424,20.9951351040557,26.7946777073925));
#61938=CARTESIAN_POINT('Ctrl Pts',(-26.6152653205548,21.0830217161674,26.7889004635225));
#61939=CARTESIAN_POINT('Ctrl Pts',(-26.684264064457,21.1740242782409,26.7831232196525));
#61940=CARTESIAN_POINT('Ctrl Pts',(-26.753183611698,21.2649223877016,26.7773526068949));
#61941=CARTESIAN_POINT('Ctrl Pts',(-26.8182266293002,21.3589289946375,26.7715819941372));
#61942=CARTESIAN_POINT('Ctrl Pts',(-26.8790990269154,21.4556714253025,26.7658113813796));
#61943=CARTESIAN_POINT('Ctrl Pts',(-26.9399328370013,21.5523525301197,26.7600444266624));
#61944=CARTESIAN_POINT('Ctrl Pts',(-26.9966010533202,21.6517656531312,26.7542774719451));
#61945=CARTESIAN_POINT('Ctrl Pts',(-27.0488517711681,21.7535075966651,26.7485105172279));
#61946=CARTESIAN_POINT('Ctrl Pts',(-27.1010828959889,21.8552113889021,26.7427457250092));
#61947=CARTESIAN_POINT('Ctrl Pts',(-27.1488996201686,21.9592418867917,26.7369809327905));
#61948=CARTESIAN_POINT('Ctrl Pts',(-27.1920954923835,22.0651704296952,26.7312161405717));
#61949=CARTESIAN_POINT('Ctrl Pts',(-27.2352863497094,22.1710866746669,26.7254520176252));
#61950=CARTESIAN_POINT('Ctrl Pts',(-27.2738572622042,22.2789001308291,26.7196878946786));
#61951=CARTESIAN_POINT('Ctrl Pts',(-27.3076498760156,22.3881620890493,26.713923771732));
#61952=CARTESIAN_POINT('Ctrl Pts',(-27.3414613438788,22.4974850082429,26.7081564327846));
#61953=CARTESIAN_POINT('Ctrl Pts',(-27.3704890617876,22.6082576355738,26.7023890938372));
#61954=CARTESIAN_POINT('Ctrl Pts',(-27.3946246312222,22.7200163241179,26.6966217548898));
#61955=CARTESIAN_POINT('Ctrl Pts',(-27.4187677948437,22.8318101772093,26.6908526012659));
#61956=CARTESIAN_POINT('Ctrl Pts',(-27.4380156707845,22.9445902890411,26.6850834476421));
#61957=CARTESIAN_POINT('Ctrl Pts',(-27.4523113303205,23.0578846488431,26.6793142940182));
#61958=CARTESIAN_POINT('Ctrl Pts',(-27.4666225286685,23.1713021550973,26.6735388695544));
#61959=CARTESIAN_POINT('Ctrl Pts',(-27.4759707289721,23.2852346002791,26.6677634450905));
#61960=CARTESIAN_POINT('Ctrl Pts',(-27.4803510307389,23.3992068836048,26.6619880206267));
#61961=CARTESIAN_POINT('Ctrl Pts',(-27.4823291632682,23.4506764610639,26.6593798544293));
#61962=CARTESIAN_POINT('Ctrl Pts',(-27.4832948486706,23.5021541814199,26.656771688232));
#61963=CARTESIAN_POINT('Ctrl Pts',(-27.4832511100809,23.5535965424957,26.6541635220347));
#61964=CARTESIAN_POINT('',(-27.4879134860282,23.5478550324797,25.4041635220347));
#61965=CARTESIAN_POINT('Ctrl Pts',(-27.4854593591317,23.5535984200475,26.6541635220347));
#61966=CARTESIAN_POINT('Ctrl Pts',(-27.487557722953,23.7854233941432,26.6424165168988));
#61967=CARTESIAN_POINT('Ctrl Pts',(-27.363218900229,25.3233322387404,26.5643738746377));
#61968=CARTESIAN_POINT('Ctrl Pts',(-25.3358175318097,27.8458907001547,26.420035595252));
#61969=CARTESIAN_POINT('Ctrl Pts',(-20.9014335845632,27.3744530235421,26.221148683877));
#61970=CARTESIAN_POINT('Ctrl Pts',(-18.9010895943725,23.3888991075444,26.0222617725022));
#61971=CARTESIAN_POINT('Ctrl Pts',(-21.1729321979881,19.5516154275727,25.8233748611272));
#61972=CARTESIAN_POINT('Ctrl Pts',(-25.6293306044078,19.3887401543539,25.6244879497525));
#61973=CARTESIAN_POINT('Ctrl Pts',(-27.4180706748919,21.9610852413708,25.4847508367215));
#61974=CARTESIAN_POINT('Ctrl Pts',(-27.4889222638918,23.4070619638991,25.4113093608156));
#61975=CARTESIAN_POINT('Ctrl Pts',(-27.4879134860282,23.5478550324797,25.4041635220347));
#61976=CARTESIAN_POINT('',(-27.4779394483698,23.5480687660733,24.1541635220347));
#61977=CARTESIAN_POINT('Ctrl Pts',(-27.4879134860282,23.5478550324797,25.4041635220347));
#61978=CARTESIAN_POINT('Ctrl Pts',(-27.4795633106279,24.7132719793335,25.3450137236907));
#61979=CARTESIAN_POINT('Ctrl Pts',(-26.3135078915754,27.199410493852,25.2195682882216));
#61980=CARTESIAN_POINT('Ctrl Pts',(-22.0830319381555,27.9647756739205,25.0278272156278));
#61981=CARTESIAN_POINT('Ctrl Pts',(-19.043145214186,24.7020921303425,24.8289403042528));
#61982=CARTESIAN_POINT('Ctrl Pts',(-20.1449079761709,20.3809656581431,24.630053392878));
#61983=CARTESIAN_POINT('Ctrl Pts',(-24.3758936586293,18.9721451101218,24.431166481503));
#61984=CARTESIAN_POINT('Ctrl Pts',(-27.1453541813937,21.2038557842603,24.2725365245553));
#61985=CARTESIAN_POINT('Ctrl Pts',(-27.4805332539196,23.031697457995,24.1802022047326));
#61986=CARTESIAN_POINT('Ctrl Pts',(-27.4779394483698,23.5480687660733,24.1541635220347));
#61987=CARTESIAN_POINT('',(-27.4799050097769,23.5534460090541,22.9041635220347));
#61988=CARTESIAN_POINT('Ctrl Pts',(-27.4779394483698,23.5480687660733,24.1541635220347));
#61989=CARTESIAN_POINT('Ctrl Pts',(-27.4739293103371,24.3464016332941,24.1139065676076));
#61990=CARTESIAN_POINT('Ctrl Pts',(-26.8489074821203,26.4652081631034,24.0073539760553));
#61991=CARTESIAN_POINT('Ctrl Pts',(-23.3829161640313,28.1992039588926,23.8345057473784));
#61992=CARTESIAN_POINT('Ctrl Pts',(-19.5485592941391,25.9224249673682,23.6356188360036));
#61993=CARTESIAN_POINT('Ctrl Pts',(-19.3914192219412,21.4658206345704,23.4367319246284));
#61994=CARTESIAN_POINT('Ctrl Pts',(-23.0558943504829,18.92463248452,23.2378450132538));
#61995=CARTESIAN_POINT('Ctrl Pts',(-26.7322134398013,20.4503798001738,23.0603222123891));
#61996=CARTESIAN_POINT('Ctrl Pts',(-27.4731489910645,22.6635309292851,22.9490950486494));
#61997=CARTESIAN_POINT('Ctrl Pts',(-27.4799050097769,23.5534460090541,22.9041635220347));
#61998=CARTESIAN_POINT('',(-27.4855853468104,23.5511498130059,21.6541638930713));
#61999=CARTESIAN_POINT('Ctrl Pts',(-27.4799050097769,23.5534460090541,22.9041635220347));
#62000=CARTESIAN_POINT('Ctrl Pts',(-27.4831173718143,23.9765841826572,22.8827994115245));
#62001=CARTESIAN_POINT('Ctrl Pts',(-27.2249116382549,25.7089597706867,22.7951396638892));
#62002=CARTESIAN_POINT('Ctrl Pts',(-24.6962908804443,28.0588384447396,22.6411842791291));
#62003=CARTESIAN_POINT('Ctrl Pts',(-20.3765858683961,26.9515156415358,22.4422973677542));
#62004=CARTESIAN_POINT('Ctrl Pts',(-18.9732114373579,22.7187204199441,22.2434104563792));
#62005=CARTESIAN_POINT('Ctrl Pts',(-21.7757497029281,19.250032706754,22.0445235450043));
#62006=CARTESIAN_POINT('Ctrl Pts',(-26.153814110843,19.7268819672536,21.8481082315933));
#62007=CARTESIAN_POINT('Ctrl Pts',(-27.4855970698216,22.2949686608996,21.717988555307));
#62008=CARTESIAN_POINT('Ctrl Pts',(-27.4895029709821,23.5511384503243,21.6541645161457));
#62009=CARTESIAN_POINT('',(-27.483250851415,23.5466170023887,20.4041635408089));
#62010=CARTESIAN_POINT('Ctrl Pts',(-27.483252427791,23.5511565794069,21.6541635220347));
#62011=CARTESIAN_POINT('Ctrl Pts',(-27.4832412653015,23.5997182533086,21.6516922554413));
#62012=CARTESIAN_POINT('Ctrl Pts',(-27.4823307347554,23.6482685215949,21.649220988848));
#62013=CARTESIAN_POINT('Ctrl Pts',(-27.4805218875495,23.6967850892526,21.6467497222546));
#62014=CARTESIAN_POINT('Ctrl Pts',(-27.4762236511744,23.8120715961606,21.6408774252859));
#62015=CARTESIAN_POINT('Ctrl Pts',(-27.4668413684358,23.9273619587229,21.6350051283172));
#62016=CARTESIAN_POINT('Ctrl Pts',(-27.4523679891428,24.0421711801925,21.6291328313485));
#62017=CARTESIAN_POINT('Ctrl Pts',(-27.4379133662,24.1568316180291,21.6232681444103));
#62018=CARTESIAN_POINT('Ctrl Pts',(-27.4183808183005,24.2710117483807,21.6174034574721));
#62019=CARTESIAN_POINT('Ctrl Pts',(-27.3938152824245,24.3842275800012,21.6115387705339));
#62020=CARTESIAN_POINT('Ctrl Pts',(-27.3692750106643,24.497326976226,21.605680115059));
#62021=CARTESIAN_POINT('Ctrl Pts',(-27.3397121336118,24.6094636447498,21.5998214595842));
#62022=CARTESIAN_POINT('Ctrl Pts',(-27.3052231850132,24.7201603881996,21.5939628041094));
#62023=CARTESIAN_POINT('Ctrl Pts',(-27.2693870677048,24.8351810439491,21.5878753043915));
#62024=CARTESIAN_POINT('Ctrl Pts',(-27.2282322570843,24.9486465408119,21.5817878046736));
#62025=CARTESIAN_POINT('Ctrl Pts',(-27.1819252516888,25.0600347195765,21.5757003049557));
#62026=CARTESIAN_POINT('Ctrl Pts',(-27.1374106575068,25.1671113817798,21.5698484348723));
#62027=CARTESIAN_POINT('Ctrl Pts',(-27.0881354790138,25.2722681324039,21.5639965647889));
#62028=CARTESIAN_POINT('Ctrl Pts',(-27.0342976388113,25.3750590122759,21.5581446947055));
#62029=CARTESIAN_POINT('Ctrl Pts',(-26.9804679959096,25.4778342413019,21.5522937156225));
#62030=CARTESIAN_POINT('Ctrl Pts',(-26.9220772643436,25.5782439497247,21.5464427365396));
#62031=CARTESIAN_POINT('Ctrl Pts',(-26.8593698902985,25.6758656919339,21.5405917574566));
#62032=CARTESIAN_POINT('Ctrl Pts',(-26.7966568782568,25.7734962112773,21.5347402523143));
#62033=CARTESIAN_POINT('Ctrl Pts',(-26.7296266756421,25.8683379182785,21.528888747172));
#62034=CARTESIAN_POINT('Ctrl Pts',(-26.6585673305653,25.9599969395348,21.5230372420297));
#62035=CARTESIAN_POINT('Ctrl Pts',(-26.5874843882269,26.0516863987566,21.5171837937299));
#62036=CARTESIAN_POINT('Ctrl Pts',(-26.5123698960616,26.1401907441226,21.5113303454302));
#62037=CARTESIAN_POINT('Ctrl Pts',(-26.4335520203143,26.2251493631483,21.5054768971304));
#62038=CARTESIAN_POINT('Ctrl Pts',(-26.3546445115273,26.3102045985721,21.4996167921889));
#62039=CARTESIAN_POINT('Ctrl Pts',(-26.2720254943442,26.3917057561524,21.4937566872473));
#62040=CARTESIAN_POINT('Ctrl Pts',(-26.1860598787519,26.4693292057808,21.4878965823058));
#62041=CARTESIAN_POINT('Ctrl Pts',(-26.1000363706979,26.5470049299443,21.4820325309503));
#62042=CARTESIAN_POINT('Ctrl Pts',(-26.0106620946121,26.6207974838015,21.4761684795949));
#62043=CARTESIAN_POINT('Ctrl Pts',(-25.9183335160132,26.6904247326581,21.4703044282395));
#62044=CARTESIAN_POINT('Ctrl Pts',(-25.8258688635199,26.7601545981808,21.4644317344429));
#62045=CARTESIAN_POINT('Ctrl Pts',(-25.7304415581211,26.8257066736033,21.4585590406463));
#62046=CARTESIAN_POINT('Ctrl Pts',(-25.6324754355502,26.8868431236994,21.4526863468497));
#62047=CARTESIAN_POINT('Ctrl Pts',(-25.6056539499634,26.9035812610477,21.4510785015264));
#62048=CARTESIAN_POINT('Ctrl Pts',(-25.5786422915133,26.9199886871719,21.4494706562031));
#62049=CARTESIAN_POINT('Ctrl Pts',(-25.5514494352447,26.9360611431222,21.4478628108797));
#62050=CARTESIAN_POINT('Ctrl Pts',(-25.4521335837017,26.9947622090686,21.441990513911));
#62051=CARTESIAN_POINT('Ctrl Pts',(-25.3500663457444,27.0491880656526,21.4361182169423));
#62052=CARTESIAN_POINT('Ctrl Pts',(-25.2456519463466,27.0990706201282,21.4302459199736));
#62053=CARTESIAN_POINT('Ctrl Pts',(-25.141372859718,27.1488885307748,21.4243812330354));
#62054=CARTESIAN_POINT('Ctrl Pts',(-25.0347530301277,27.1941746713993,21.4185165460972));
#62055=CARTESIAN_POINT('Ctrl Pts',(-24.9262239378743,27.2347052304508,21.412651859159));
#62056=CARTESIAN_POINT('Ctrl Pts',(-24.8178064609984,27.2751941063595,21.4067932036842));
#62057=CARTESIAN_POINT('Ctrl Pts',(-24.7074840120062,27.3109369850299,21.4009345482094));
#62058=CARTESIAN_POINT('Ctrl Pts',(-24.5957102456366,27.3417571365125,21.3950758927345));
#62059=CARTESIAN_POINT('Ctrl Pts',(-24.4795704975035,27.3737811502581,21.3889883930166));
#62060=CARTESIAN_POINT('Ctrl Pts',(-24.3618641514241,27.4004898287756,21.3829008932987));
#62061=CARTESIAN_POINT('Ctrl Pts',(-24.2431205082215,27.4217410008883,21.3768133935808));
#62062=CARTESIAN_POINT('Ctrl Pts',(-24.1289730904882,27.4421696011489,21.3709615234974));
#62063=CARTESIAN_POINT('Ctrl Pts',(-24.0138676289437,27.457555248355,21.365109653414));
#62064=CARTESIAN_POINT('Ctrl Pts',(-23.8982863020791,27.4678233982736,21.3592577833306));
#62065=CARTESIAN_POINT('Ctrl Pts',(-23.7827225735224,27.478089984773,21.3534068042477));
#62066=CARTESIAN_POINT('Ctrl Pts',(-23.6666835353571,27.4832405866847,21.3475558251647));
#62067=CARTESIAN_POINT('Ctrl Pts',(-23.5506567316891,27.4832525109241,21.3417048460817));
#62068=CARTESIAN_POINT('Ctrl Pts',(-23.4346194960948,27.4832644362356,21.3358533409394));
#62069=CARTESIAN_POINT('Ctrl Pts',(-23.3185949105921,27.4781367653861,21.3300018357971));
#62070=CARTESIAN_POINT('Ctrl Pts',(-23.2030700496983,27.4678989328125,21.3241503306548));
#62071=CARTESIAN_POINT('Ctrl Pts',(-23.087506825513,27.4576577004775,21.3182968823551));
#62072=CARTESIAN_POINT('Ctrl Pts',(-22.9724440674643,27.4423029685653,21.3124434340553));
#62073=CARTESIAN_POINT('Ctrl Pts',(-22.8583625526531,27.4219159025082,21.3065899857555));
#62074=CARTESIAN_POINT('Ctrl Pts',(-22.7441513023872,27.40150565193,21.300729880814));
#62075=CARTESIAN_POINT('Ctrl Pts',(-22.6309239298121,27.376051717323,21.2948697758725));
#62076=CARTESIAN_POINT('Ctrl Pts',(-22.5191499596855,27.3456861677886,21.2890096709309));
#62077=CARTESIAN_POINT('Ctrl Pts',(-22.4073007167856,27.3153001689572,21.2831456195755));
#62078=CARTESIAN_POINT('Ctrl Pts',(-22.2969072180469,27.2799960945907,21.27728156822));
#62079=CARTESIAN_POINT('Ctrl Pts',(-22.1884211345414,27.2399549920193,21.2714175168646));
#62080=CARTESIAN_POINT('Ctrl Pts',(-22.0797751642049,27.1998548768557,21.265544823068));
#62081=CARTESIAN_POINT('Ctrl Pts',(-21.9730425992842,27.1550039594364,21.2596721292714));
#62082=CARTESIAN_POINT('Ctrl Pts',(-21.8686526357277,27.1056302598527,21.2537994354748));
#62083=CARTESIAN_POINT('Ctrl Pts',(-21.8400724099367,27.0921125668278,21.2521915901515));
#62084=CARTESIAN_POINT('Ctrl Pts',(-21.8116676205528,27.0782561147456,21.2505837448282));
#62085=CARTESIAN_POINT('Ctrl Pts',(-21.783446702094,27.0640661523193,21.2489758995048));
#62086=CARTESIAN_POINT('Ctrl Pts',(-21.6803760823553,27.0122404747291,21.2431036025361));
#62087=CARTESIAN_POINT('Ctrl Pts',(-21.5794150269874,26.9557890776857,21.2372313055674));
#62088=CARTESIAN_POINT('Ctrl Pts',(-21.4810075876501,26.8949071269474,21.2313590085987));
#62089=CARTESIAN_POINT('Ctrl Pts',(-21.3827276765389,26.834104074382,21.2254943216605));
#62090=CARTESIAN_POINT('Ctrl Pts',(-21.2869951487804,26.7688821016771,21.2196296347223));
#62091=CARTESIAN_POINT('Ctrl Pts',(-21.1942315341809,26.6994832408161,21.2137649477841));
#62092=CARTESIAN_POINT('Ctrl Pts',(-21.1015633211519,26.630155752339,21.2079062923092));
#62093=CARTESIAN_POINT('Ctrl Pts',(-21.0118582770428,26.5566601661541,21.2020476368344));
#62094=CARTESIAN_POINT('Ctrl Pts',(-20.9255103073432,26.4792826195747,21.1961889813596));
#62095=CARTESIAN_POINT('Ctrl Pts',(-20.835789509893,26.3988826378727,21.1901014816417));
#62096=CARTESIAN_POINT('Ctrl Pts',(-20.7496937805493,26.31429148701,21.1840139819238));
#62097=CARTESIAN_POINT('Ctrl Pts',(-20.6676288398422,26.2258776271016,21.1779264822059));
#62098=CARTESIAN_POINT('Ctrl Pts',(-20.5887403973494,26.1408860138395,21.1720746121225));
#62099=CARTESIAN_POINT('Ctrl Pts',(-20.513576812579,26.0523624523329,21.1662227420391));
#62100=CARTESIAN_POINT('Ctrl Pts',(-20.4424614387603,25.9606723131183,21.1603708719557));
#62101=CARTESIAN_POINT('Ctrl Pts',(-20.3713568929038,25.868996134561,21.1545198928727));
#62102=CARTESIAN_POINT('Ctrl Pts',(-20.3042995857251,25.7741546635035,21.1486689137897));
#62103=CARTESIAN_POINT('Ctrl Pts',(-20.2415721475544,25.676545812408,21.1428179347067));
#62104=CARTESIAN_POINT('Ctrl Pts',(-20.1788390695834,25.5789281853374,21.1369664295644));
#62105=CARTESIAN_POINT('Ctrl Pts',(-20.1204368580069,25.4785430313931,21.1311149244221));
#62106=CARTESIAN_POINT('Ctrl Pts',(-20.0666040335643,25.3758160450997,21.1252634192798));
#62107=CARTESIAN_POINT('Ctrl Pts',(-20.0127533324127,25.2730549454104,21.11940997098));
#62108=CARTESIAN_POINT('Ctrl Pts',(-19.963475227414,25.1679508329805,21.1135565226803));
#62109=CARTESIAN_POINT('Ctrl Pts',(-19.9189613131329,25.0609520670088,21.1077030743805));
#62110=CARTESIAN_POINT('Ctrl Pts',(-19.8743967768653,24.9538316202058,21.1018429694389));
#62111=CARTESIAN_POINT('Ctrl Pts',(-19.8346074041967,24.8448126011775,21.0959828644974));
#62112=CARTESIAN_POINT('Ctrl Pts',(-19.7997358812123,24.7343614179281,21.0901227595558));
#62113=CARTESIAN_POINT('Ctrl Pts',(-19.7648408744397,24.6238358527198,21.0842587082004));
#62114=CARTESIAN_POINT('Ctrl Pts',(-19.734870418564,24.5118766011805,21.0783946568449));
#62115=CARTESIAN_POINT('Ctrl Pts',(-19.7099163427907,24.3989615255183,21.0725306054895));
#62116=CARTESIAN_POINT('Ctrl Pts',(-19.684925489691,24.2858800355745,21.0666579116929));
#62117=CARTESIAN_POINT('Ctrl Pts',(-19.6649658429815,24.1718403156909,21.0607852178963));
#62118=CARTESIAN_POINT('Ctrl Pts',(-19.6500775641385,24.0573267101454,21.0549125240998));
#62119=CARTESIAN_POINT('Ctrl Pts',(-19.6460014024419,24.0259748005267,21.0533046787765));
#62120=CARTESIAN_POINT('Ctrl Pts',(-19.6423050752392,23.9945873748693,21.0516968334532));
#62121=CARTESIAN_POINT('Ctrl Pts',(-19.6389887259146,23.9631743664267,21.0500889881299));
#62122=CARTESIAN_POINT('Ctrl Pts',(-19.626876498573,23.8484453489128,21.0442166911612));
#62123=CARTESIAN_POINT('Ctrl Pts',(-19.6197962755918,23.7329907458361,21.0383443941925));
#62124=CARTESIAN_POINT('Ctrl Pts',(-19.6178238894911,23.6172896406746,21.0324720972238));
#62125=CARTESIAN_POINT('Ctrl Pts',(-19.6158540594461,23.5017384749566,21.0266074102856));
#62126=CARTESIAN_POINT('Ctrl Pts',(-19.6189789097497,23.385941851927,21.0207427233475));
#62127=CARTESIAN_POINT('Ctrl Pts',(-19.6272226695634,23.270385240232,21.0148780364093));
#62128=CARTESIAN_POINT('Ctrl Pts',(-19.6354579511863,23.1549474712782,21.0090193809345));
#62129=CARTESIAN_POINT('Ctrl Pts',(-19.648801641763,23.0397496325442,21.0031607254597));
#62130=CARTESIAN_POINT('Ctrl Pts',(-19.6672259317868,22.9252777926755,20.9973020699848));
#62131=CARTESIAN_POINT('Ctrl Pts',(-19.6863698908069,22.8063345819157,20.9912145702669));
#62132=CARTESIAN_POINT('Ctrl Pts',(-19.7109994537516,22.6881756971685,20.985127070549));
#62133=CARTESIAN_POINT('Ctrl Pts',(-19.7410239380902,22.5713416462355,20.9790395708311));
#62134=CARTESIAN_POINT('Ctrl Pts',(-19.7698862608518,22.4590299059386,20.9731877007477));
#62135=CARTESIAN_POINT('Ctrl Pts',(-19.8037335144383,22.347942783184,20.9673358306644));
#62136=CARTESIAN_POINT('Ctrl Pts',(-19.8424330926155,22.2385498187329,20.961483960581));
#62137=CARTESIAN_POINT('Ctrl Pts',(-19.88112677843,22.1291735103553,20.955632981498));
#62138=CARTESIAN_POINT('Ctrl Pts',(-19.9246711820129,22.0214912370001,20.9497820024151));
#62139=CARTESIAN_POINT('Ctrl Pts',(-19.9728843066086,21.9159558688609,20.9439310233321));
#62140=CARTESIAN_POINT('Ctrl Pts',(-20.0211017660281,21.8104110120766,20.9380795181898));
#62141=CARTESIAN_POINT('Ctrl Pts',(-20.0739886091254,21.7070138202552,20.9322280130475));
#62142=CARTESIAN_POINT('Ctrl Pts',(-20.1313156225259,21.6061950708339,20.9263765079053));
#62143=CARTESIAN_POINT('Ctrl Pts',(-20.1886616729795,21.5053428417007,20.9205230596055));
#62144=CARTESIAN_POINT('Ctrl Pts',(-20.2504506214302,21.4070711167174,20.9146696113058));
#62145=CARTESIAN_POINT('Ctrl Pts',(-20.3164088207457,21.3117834447602,20.908816163006));
#62146=CARTESIAN_POINT('Ctrl Pts',(-20.3824420288565,21.2163874100286,20.9029560580645));
#62147=CARTESIAN_POINT('Ctrl Pts',(-20.452653715994,21.1239825417778,20.8970959531229));
#62148=CARTESIAN_POINT('Ctrl Pts',(-20.5267286131565,21.0349409975039,20.8912358481814));
#62149=CARTESIAN_POINT('Ctrl Pts',(-20.6008533951262,20.9458394893228,20.885371796826));
#62150=CARTESIAN_POINT('Ctrl Pts',(-20.6788462899871,20.8601061201963,20.8795077454705));
#62151=CARTESIAN_POINT('Ctrl Pts',(-20.7603549018245,20.7780764523574,20.8736436941151));
#62152=CARTESIAN_POINT('Ctrl Pts',(-20.841983641085,20.6959258891628,20.8677710003186));
#62153=CARTESIAN_POINT('Ctrl Pts',(-20.9271381356132,20.6174902004143,20.861898306522));
#62154=CARTESIAN_POINT('Ctrl Pts',(-21.015432607422,20.5430649832508,20.8560256127254));
#62155=CARTESIAN_POINT('Ctrl Pts',(-21.0396061568191,20.5226886037717,20.854417767402));
#62156=CARTESIAN_POINT('Ctrl Pts',(-21.0640149031018,20.5026125875007,20.8528099220785));
#62157=CARTESIAN_POINT('Ctrl Pts',(-21.0886505667624,20.4828424244141,20.8512020767551));
#62158=CARTESIAN_POINT('Ctrl Pts',(-21.1786268417969,20.4106363066548,20.8453297797864));
#62159=CARTESIAN_POINT('Ctrl Pts',(-21.2719335758181,20.3422714888359,20.8394574828176));
#62160=CARTESIAN_POINT('Ctrl Pts',(-21.3682086985497,20.2780707350582,20.8335851858489));
#62161=CARTESIAN_POINT('Ctrl Pts',(-21.4643590563682,20.2139531803587,20.8277204989107));
#62162=CARTESIAN_POINT('Ctrl Pts',(-21.5634698122484,20.1539891856337,20.8218558119725));
#62163=CARTESIAN_POINT('Ctrl Pts',(-21.6651456301621,20.0984615516671,20.8159911250343));
#62164=CARTESIAN_POINT('Ctrl Pts',(-21.7667168808622,20.042991024396,20.8101324695595));
#62165=CARTESIAN_POINT('Ctrl Pts',(-21.8708475858432,19.9919479797429,20.8042738140847));
#62166=CARTESIAN_POINT('Ctrl Pts',(-21.9771137751809,19.9455717618124,20.7984151586099));
#62167=CARTESIAN_POINT('Ctrl Pts',(-22.087530815472,19.8973840479619,20.7923276588919));
#62168=CARTESIAN_POINT('Ctrl Pts',(-22.2002531906017,19.8542354261917,20.786240159174));
#62169=CARTESIAN_POINT('Ctrl Pts',(-22.3147771445353,19.8163417711477,20.7801526594561));
#62170=CARTESIAN_POINT('Ctrl Pts',(-22.424868205055,19.7799148706831,20.7743007893727));
#62171=CARTESIAN_POINT('Ctrl Pts',(-22.5366235407265,19.7483438338567,20.7684489192893));
#62172=CARTESIAN_POINT('Ctrl Pts',(-22.6495764397381,19.7217709035055,20.7625970492059));
#62173=CARTESIAN_POINT('Ctrl Pts',(-22.7625121406436,19.6952020191245,20.756746070123));
#62174=CARTESIAN_POINT('Ctrl Pts',(-22.8766446400523,19.6736298227336,20.75089509104));
#62175=CARTESIAN_POINT('Ctrl Pts',(-22.9914945537099,19.6571459929467,20.745044111957));
#62176=CARTESIAN_POINT('Ctrl Pts',(-23.10635479348,19.6406606811048,20.7391926068147));
#62177=CARTESIAN_POINT('Ctrl Pts',(-23.2219321665099,19.6292647040536,20.7333411016724));
#62178=CARTESIAN_POINT('Ctrl Pts',(-23.3377403529678,19.6229980742019,20.7274895965301));
#62179=CARTESIAN_POINT('Ctrl Pts',(-23.4535869968036,19.6167293633389,20.7216361482303));
#62180=CARTESIAN_POINT('Ctrl Pts',(-23.5696641939169,19.6155934089932,20.7157826999306));
#62181=CARTESIAN_POINT('Ctrl Pts',(-23.6854845139918,19.6195781225166,20.7099292516308));
#62182=CARTESIAN_POINT('Ctrl Pts',(-23.8014365469203,19.6235673675244,20.7040691466892));
#62183=CARTESIAN_POINT('Ctrl Pts',(-23.9171307063542,19.6326888893325,20.6982090417477));
#62184=CARTESIAN_POINT('Ctrl Pts',(-24.0320834736873,19.6468786137435,20.6923489368062));
#62185=CARTESIAN_POINT('Ctrl Pts',(-24.1471136545145,19.6610778940458,20.6864848854507));
#62186=CARTESIAN_POINT('Ctrl Pts',(-24.2614010424423,19.6803521045682,20.6806208340953));
#62187=CARTESIAN_POINT('Ctrl Pts',(-24.3744728384027,19.7045861543274,20.6747567827398));
#62188=CARTESIAN_POINT('Ctrl Pts',(-24.4877112796192,19.7288559202384,20.6688840889432));
#62189=CARTESIAN_POINT('Ctrl Pts',(-24.5997301548246,19.7581000103351,20.6630113951467));
#62190=CARTESIAN_POINT('Ctrl Pts',(-24.7100722438301,19.7921536459089,20.6571387013501));
#62191=CARTESIAN_POINT('Ctrl Pts',(-24.740282062002,19.8014769616812,20.6555308560268));
#62192=CARTESIAN_POINT('Ctrl Pts',(-24.7703663134547,19.8111605115869,20.6539230107035));
#62193=CARTESIAN_POINT('Ctrl Pts',(-24.8003159039542,19.821200297502,20.6523151653801));
#62194=CARTESIAN_POINT('Ctrl Pts',(-24.9097001133387,19.8578683796494,20.6464428684114));
#62195=CARTESIAN_POINT('Ctrl Pts',(-25.0176528269035,19.8994148182835,20.6405705714427));
#62196=CARTESIAN_POINT('Ctrl Pts',(-25.1237067834616,19.9457094652855,20.634698274474));
#62197=CARTESIAN_POINT('Ctrl Pts',(-25.2296233025146,19.9919441181016,20.6288335875358));
#62198=CARTESIAN_POINT('Ctrl Pts',(-25.3336455825241,20.0429145787256,20.6229689005975));
#62199=CARTESIAN_POINT('Ctrl Pts',(-25.435322002563,20.0984411101362,20.6171042136593));
#62200=CARTESIAN_POINT('Ctrl Pts',(-25.5368938547689,20.1539105359852,20.6112455581845));
#62201=CARTESIAN_POINT('Ctrl Pts',(-25.6361242851046,20.2139265157134,20.6053869027097));
#62202=CARTESIAN_POINT('Ctrl Pts',(-25.7325827556419,20.2782617319448,20.5995282472348));
#62203=CARTESIAN_POINT('Ctrl Pts',(-25.8328089789975,20.3451099383878,20.5934407475169));
#62204=CARTESIAN_POINT('Ctrl Pts',(-25.9300418608491,20.4166215046015,20.587353247799));
#62205=CARTESIAN_POINT('Ctrl Pts',(-26.0238274807427,20.4924893015798,20.5812657480811));
#62206=CARTESIAN_POINT('Ctrl Pts',(-26.1139829285855,20.5654204739831,20.5754138779977));
#62207=CARTESIAN_POINT('Ctrl Pts',(-26.2009526681496,20.6423766291465,20.5695620079143));
#62208=CARTESIAN_POINT('Ctrl Pts',(-26.2843647506304,20.7230420028754,20.5637101378309));
#62209=CARTESIAN_POINT('Ctrl Pts',(-26.3677641328631,20.8036950945677,20.5578591587479));
#62210=CARTESIAN_POINT('Ctrl Pts',(-26.447606637981,20.8880559946041,20.5520081796649));
#62211=CARTESIAN_POINT('Ctrl Pts',(-26.5235560077159,20.9757709451457,20.5461572005819));
#62212=CARTESIAN_POINT('Ctrl Pts',(-26.5995122060301,21.0634937821056,20.5403056954396));
#62213=CARTESIAN_POINT('Ctrl Pts',(-26.6715743025231,21.1545709565156,20.5344541902973));
#62214=CARTESIAN_POINT('Ctrl Pts',(-26.7394457575984,21.2486149477451,20.528602685155));
#62215=CARTESIAN_POINT('Ctrl Pts',(-26.8073397513064,21.3426901689369,20.5227492368552));
#62216=CARTESIAN_POINT('Ctrl Pts',(-26.8710400946581,21.43973383096,20.5168957885554));
#62217=CARTESIAN_POINT('Ctrl Pts',(-26.9302934812866,21.5393293160844,20.5110423402556));
#62218=CARTESIAN_POINT('Ctrl Pts',(-26.9896142518824,21.6390380629022,20.5051822353141));
#62219=CARTESIAN_POINT('Ctrl Pts',(-27.0444777603398,21.7413040696055,20.4993221303725));
#62220=CARTESIAN_POINT('Ctrl Pts',(-27.0946765510513,21.8456859090583,20.493462025431));
#62221=CARTESIAN_POINT('Ctrl Pts',(-27.1449091475065,21.9501380431469,20.4875979740755));
#62222=CARTESIAN_POINT('Ctrl Pts',(-27.1904706089677,22.0567084680319,20.4817339227201));
#62223=CARTESIAN_POINT('Ctrl Pts',(-27.2312021954705,22.1649371983693,20.4758698713646));
#62224=CARTESIAN_POINT('Ctrl Pts',(-27.2719938122011,22.2733254362509,20.469997177568));
#62225=CARTESIAN_POINT('Ctrl Pts',(-27.3079412194039,22.3833764658842,20.4641244837714));
#62226=CARTESIAN_POINT('Ctrl Pts',(-27.3389359012759,22.4946165503754,20.4582517899748));
#62227=CARTESIAN_POINT('Ctrl Pts',(-27.3474217266942,22.5250722246876,20.4566439446516));
#62228=CARTESIAN_POINT('Ctrl Pts',(-27.3555366069571,22.5556169794325,20.4550360993284));
#62229=CARTESIAN_POINT('Ctrl Pts',(-27.3632789899344,22.5862410023232,20.4534282540052));
#62230=CARTESIAN_POINT('Ctrl Pts',(-27.4005143394058,22.7335207478353,20.4456956628015));
#62231=CARTESIAN_POINT('Ctrl Pts',(-27.4292315992316,22.8830345880011,20.4379630715977));
#62232=CARTESIAN_POINT('Ctrl Pts',(-27.4492142270171,23.0339321869424,20.430230480394));
#62233=CARTESIAN_POINT('Ctrl Pts',(-27.4687344541642,23.1813379955728,20.4226768223691));
#62234=CARTESIAN_POINT('Ctrl Pts',(-27.4799196555139,23.3300645645562,20.4151231643441));
#62235=CARTESIAN_POINT('Ctrl Pts',(-27.4826124151087,23.4792965783715,20.4075695063192));
#62236=CARTESIAN_POINT('Ctrl Pts',(-27.4830171393839,23.501726289045,20.4064341844824));
#62237=CARTESIAN_POINT('Ctrl Pts',(-27.4832300997421,23.5241673704898,20.4052988626457));
#62238=CARTESIAN_POINT('Ctrl Pts',(-27.483250851415,23.5466170023887,20.4041635408089));
#62239=CARTESIAN_POINT('',(-27.4768438131603,23.5509604052536,19.1541635220348));
#62240=CARTESIAN_POINT('Ctrl Pts',(-27.482652284421,23.5466179268635,20.4041635220348));
#62241=CARTESIAN_POINT('Ctrl Pts',(-27.4736509478652,24.5326769039293,20.3542894622333));
#62242=CARTESIAN_POINT('Ctrl Pts',(-26.5977887904392,26.8437168577948,20.2381197653068));
#62243=CARTESIAN_POINT('Ctrl Pts',(-22.7128308123558,28.1262197186493,20.0556544312555));
#62244=CARTESIAN_POINT('Ctrl Pts',(-19.2477526204729,25.3192198423143,19.8567675198806));
#62245=CARTESIAN_POINT('Ctrl Pts',(-19.7363070551659,20.8866889912118,19.6578806085056));
#62246=CARTESIAN_POINT('Ctrl Pts',(-23.7295540135405,18.9017472008686,19.4589936971309));
#62247=CARTESIAN_POINT('Ctrl Pts',(-26.9616635618324,20.8321907758035,19.2910880016405));
#62248=CARTESIAN_POINT('Ctrl Pts',(-27.4757215964172,22.8501543544342,19.1894779432751));
#62249=CARTESIAN_POINT('Ctrl Pts',(-27.4768438131603,23.5509604052536,19.1541635220348));
#62250=CARTESIAN_POINT('',(-27.4852583988885,23.553643346945,17.9041635220348));
#62251=CARTESIAN_POINT('Ctrl Pts',(-27.4768438131603,23.5509604052536,19.1541635220348));
#62252=CARTESIAN_POINT('Ctrl Pts',(-27.4778283299092,24.165775055786,19.1231823061502));
#62253=CARTESIAN_POINT('Ctrl Pts',(-27.0518825353482,26.0949196521075,19.0259054531406));
#62254=CARTESIAN_POINT('Ctrl Pts',(-24.0327034582734,28.1771296573096,18.8623329630062));
#62255=CARTESIAN_POINT('Ctrl Pts',(-19.9183683533861,26.4571698245448,18.6634460516312));
#62256=CARTESIAN_POINT('Ctrl Pts',(-19.1414268753694,22.0659994655903,18.4645591402563));
#62257=CARTESIAN_POINT('Ctrl Pts',(-22.4158223687412,19.0387318304797,18.2656722288814));
#62258=CARTESIAN_POINT('Ctrl Pts',(-26.4702848712463,20.0891904388618,18.0788736894743));
#62259=CARTESIAN_POINT('Ctrl Pts',(-27.4755052834716,22.4837319727721,17.958370787192));
#62260=CARTESIAN_POINT('Ctrl Pts',(-27.4852583988885,23.553643346945,17.9041635220348));
#62261=CARTESIAN_POINT('',(-27.4880679510806,23.5479486834992,16.6541635220348));
#62262=CARTESIAN_POINT('Ctrl Pts',(-27.4852583988885,23.553643346945,17.9041635220348));
#62263=CARTESIAN_POINT('Ctrl Pts',(-27.4874333709454,23.792236580268,17.8920751500671));
#62264=CARTESIAN_POINT('Ctrl Pts',(-27.3588666602939,25.3369952882741,17.8136911409746));
#62265=CARTESIAN_POINT('Ctrl Pts',(-25.313681394457,27.8550254035316,17.6690114947566));
#62266=CARTESIAN_POINT('Ctrl Pts',(-20.8817829454537,27.3607670506816,17.470124583382));
#62267=CARTESIAN_POINT('Ctrl Pts',(-18.9019817972975,23.3649689332391,17.271237672007));
#62268=CARTESIAN_POINT('Ctrl Pts',(-21.1935473456834,19.539430733317,17.0723507606322));
#62269=CARTESIAN_POINT('Ctrl Pts',(-25.6507251443653,19.3994977044937,16.8734638492572));
#62270=CARTESIAN_POINT('Ctrl Pts',(-27.4218625880093,21.9747100905248,16.7340681030581));
#62271=CARTESIAN_POINT('Ctrl Pts',(-27.4889989329917,23.4138953184574,16.6609679939839));
#62272=CARTESIAN_POINT('Ctrl Pts',(-27.4880679510806,23.5479486834992,16.6541635220348));
#62273=CARTESIAN_POINT('',(-27.4814458092685,23.5479673557521,15.4041640332968));
#62274=CARTESIAN_POINT('Ctrl Pts',(-27.4880679510806,23.5479486834992,16.6541635220348));
#62275=CARTESIAN_POINT('Ctrl Pts',(-27.4799284218034,24.7199706922043,16.594672356859));
#62276=CARTESIAN_POINT('Ctrl Pts',(-26.3022252840322,27.2122626367951,16.4688855545583));
#62277=CARTESIAN_POINT('Ctrl Pts',(-22.0603268787045,27.9571644187965,16.2768031151325));
#62278=CARTESIAN_POINT('Ctrl Pts',(-19.0372756429476,24.678875778727,16.0779162037576));
#62279=CARTESIAN_POINT('Ctrl Pts',(-20.1612675306071,20.3634780661081,15.8790292923827));
#62280=CARTESIAN_POINT('Ctrl Pts',(-24.3994492957219,18.9764558934434,15.680142381008));
#62281=CARTESIAN_POINT('Ctrl Pts',(-27.1514415008424,21.2175531301115,15.5218542812444));
#62282=CARTESIAN_POINT('Ctrl Pts',(-27.4807207713122,23.038395923409,15.429861818606));
#62283=CARTESIAN_POINT('Ctrl Pts',(-27.4780552727636,23.5479502857209,15.4041649930927));
#62284=CARTESIAN_POINT('',(-27.4822862170138,23.553399450288,14.1541631347917));
#62285=CARTESIAN_POINT('Ctrl Pts',(-27.4832518730933,23.5479764485802,15.4041635220348));
#62286=CARTESIAN_POINT('Ctrl Pts',(-27.4833198073102,23.6653646180412,15.3982514394489));
#62287=CARTESIAN_POINT('Ctrl Pts',(-27.4781278759661,23.7827617822172,15.392339356863));
#62288=CARTESIAN_POINT('Ctrl Pts',(-27.4677002237111,23.8996700188229,15.3864272742771));
#62289=CARTESIAN_POINT('Ctrl Pts',(-27.4572706033443,24.016600320653,15.3805140758466));
#62290=CARTESIAN_POINT('Ctrl Pts',(-27.441603330606,24.1330411114468,15.374600877416));
#62291=CARTESIAN_POINT('Ctrl Pts',(-27.4207744155021,24.2484998710837,15.3686876789855));
#62292=CARTESIAN_POINT('Ctrl Pts',(-27.3999369283831,24.3640061470802,15.3627720470136));
#62293=CARTESIAN_POINT('Ctrl Pts',(-27.373933642155,24.4785291927818,15.3568564150417));
#62294=CARTESIAN_POINT('Ctrl Pts',(-27.3428915187345,24.591587498927,15.3509407830699));
#62295=CARTESIAN_POINT('Ctrl Pts',(-27.3118073488031,24.7047989423829,15.3450171383831));
#62296=CARTESIAN_POINT('Ctrl Pts',(-27.2756708155007,24.8165412958034,15.3390934936964));
#62297=CARTESIAN_POINT('Ctrl Pts',(-27.2346586971704,24.9263485340869,15.3331698490096));
#62298=CARTESIAN_POINT('Ctrl Pts',(-27.1936177556452,25.0362329445708,15.327242041203));
#62299=CARTESIAN_POINT('Ctrl Pts',(-27.1476945583824,25.1441791610812,15.3213142333964));
#62300=CARTESIAN_POINT('Ctrl Pts',(-27.0971131938648,25.2497431739592,15.3153864255898));
#62301=CARTESIAN_POINT('Ctrl Pts',(-27.0464387821752,25.3555013775826,15.3094477132582));
#62302=CARTESIAN_POINT('Ctrl Pts',(-26.9910892698278,25.4588682669344,15.3035090009267));
#62303=CARTESIAN_POINT('Ctrl Pts',(-26.9313340448883,25.559425695246,15.2975702885951));
#62304=CARTESIAN_POINT('Ctrl Pts',(-26.8803475254188,25.6452269499749,15.2925030451494));
#62305=CARTESIAN_POINT('Ctrl Pts',(-26.8261542681029,25.7289831563621,15.2874358017038));
#62306=CARTESIAN_POINT('Ctrl Pts',(-26.7689449230318,25.8104534718642,15.2823685582581));
#62307=CARTESIAN_POINT('Ctrl Pts',(-26.702646497222,25.9048673068994,15.2764962612894));
#62308=CARTESIAN_POINT('Ctrl Pts',(-26.6320793230445,25.9965197419879,15.2706239643207));
#62309=CARTESIAN_POINT('Ctrl Pts',(-26.5575012184891,26.0849999226131,15.264751667352));
#62310=CARTESIAN_POINT('Ctrl Pts',(-26.4830197612344,26.1733654399512,15.2588869804138));
#62311=CARTESIAN_POINT('Ctrl Pts',(-26.4045379742129,26.258566564946,15.2530222934756));
#62312=CARTESIAN_POINT('Ctrl Pts',(-26.3223567574976,26.3402215568418,15.2471576065374));
#62313=CARTESIAN_POINT('Ctrl Pts',(-26.2402600590189,26.4217925716903,15.2412989510626));
#62314=CARTESIAN_POINT('Ctrl Pts',(-26.1544717899351,26.4998244178487,15.2354402955878));
#62315=CARTESIAN_POINT('Ctrl Pts',(-26.065332457127,26.5739691137642,15.229581640113));
#62316=CARTESIAN_POINT('Ctrl Pts',(-25.9727112634665,26.6510099668079,15.2234941403951));
#62317=CARTESIAN_POINT('Ctrl Pts',(-25.8764721712179,26.7238534602628,15.2174066406772));
#62318=CARTESIAN_POINT('Ctrl Pts',(-25.7770388530061,26.7921519254475,15.2113191409593));
#62319=CARTESIAN_POINT('Ctrl Pts',(-25.6814543130309,26.8578067531562,15.2054672708759));
#62320=CARTESIAN_POINT('Ctrl Pts',(-25.5829186002999,26.9192616043388,15.1996154007925));
#62321=CARTESIAN_POINT('Ctrl Pts',(-25.4818403227033,26.9762498471666,15.1937635307091));
#62322=CARTESIAN_POINT('Ctrl Pts',(-25.3807774351936,27.0332294130164,15.1879125516261));
#62323=CARTESIAN_POINT('Ctrl Pts',(-25.2771731125486,27.0857435197654,15.1820615725432));
#62324=CARTESIAN_POINT('Ctrl Pts',(-25.171462219991,27.1335705676174,15.1762105934602));
#62325=CARTESIAN_POINT('Ctrl Pts',(-25.0657418230066,27.1814019155813,15.1703590883179));
#62326=CARTESIAN_POINT('Ctrl Pts',(-24.9579148562495,27.2245451965112,15.1645075831756));
#62327=CARTESIAN_POINT('Ctrl Pts',(-24.8484372395267,27.2628264992199,15.1586560780333));
#62328=CARTESIAN_POINT('Ctrl Pts',(-24.7389232676711,27.3011205143158,15.1528026297336));
#62329=CARTESIAN_POINT('Ctrl Pts',(-24.6277579459064,27.3345492043703,15.1469491814338));
#62330=CARTESIAN_POINT('Ctrl Pts',(-24.515412775287,27.3629883872431,15.1410957331341));
#62331=CARTESIAN_POINT('Ctrl Pts',(-24.4029398438132,27.3914599116422,15.1352356281925));
#62332=CARTESIAN_POINT('Ctrl Pts',(-24.2892847863837,27.4149305019169,15.129375523251));
#62333=CARTESIAN_POINT('Ctrl Pts',(-24.174929829752,27.4333269931604,15.1235154183095));
#62334=CARTESIAN_POINT('Ctrl Pts',(-24.0604978622143,27.4517358732894,15.1176513669541));
#62335=CARTESIAN_POINT('Ctrl Pts',(-23.9453654665833,27.4650638028659,15.1117873155986));
#62336=CARTESIAN_POINT('Ctrl Pts',(-23.8300187871143,27.4732896003858,15.1059232642432));
#62337=CARTESIAN_POINT('Ctrl Pts',(-23.714502109665,27.4815275210892,15.1000505704467));
#62338=CARTESIAN_POINT('Ctrl Pts',(-23.5987709297598,27.4846482911153,15.0941778766501));
#62339=CARTESIAN_POINT('Ctrl Pts',(-23.4833102719325,27.4826827896718,15.0883051828535));
#62340=CARTESIAN_POINT('Ctrl Pts',(-23.4516990752384,27.4821446682554,15.0866973375301));
#62341=CARTESIAN_POINT('Ctrl Pts',(-23.4201081172826,27.4812255927403,15.0850894922067));
#62342=CARTESIAN_POINT('Ctrl Pts',(-23.3885472460941,27.4799268694236,15.0834816468833));
#62343=CARTESIAN_POINT('Ctrl Pts',(-23.27327819284,27.4751835717416,15.0776093499146));
#62344=CARTESIAN_POINT('Ctrl Pts',(-23.1580249122346,27.4653562507003,15.0717370529458));
#62345=CARTESIAN_POINT('Ctrl Pts',(-23.0432724246296,27.450439728617,15.0658647559771));
#62346=CARTESIAN_POINT('Ctrl Pts',(-22.9286686471352,27.4355425371617,15.0600000690389));
#62347=CARTESIAN_POINT('Ctrl Pts',(-22.8145647781872,27.4155693129454,15.0541353821007));
#62348=CARTESIAN_POINT('Ctrl Pts',(-22.7014446319339,27.3905668611866,15.0482706951625));
#62349=CARTESIAN_POINT('Ctrl Pts',(-22.5884408226691,27.3655901228841,15.0424120396877));
#62350=CARTESIAN_POINT('Ctrl Pts',(-22.4764191249956,27.3355945335804,15.0365533842129));
#62351=CARTESIAN_POINT('Ctrl Pts',(-22.3658563600363,27.3006784686462,15.030694728738));
#62352=CARTESIAN_POINT('Ctrl Pts',(-22.2509749160955,27.264398551462,15.0246072290201));
#62353=CARTESIAN_POINT('Ctrl Pts',(-22.1376691536408,27.2228059846972,15.0185197293022));
#62354=CARTESIAN_POINT('Ctrl Pts',(-22.0264605851813,27.1760692815786,15.0124322295843));
#62355=CARTESIAN_POINT('Ctrl Pts',(-21.919556581084,27.1311416220386,15.0065803595009));
#62356=CARTESIAN_POINT('Ctrl Pts',(-21.8145908537228,27.0814608259816,15.0007284894175));
#62357=CARTESIAN_POINT('Ctrl Pts',(-21.7120085948154,27.0272265362747,14.9948766193341));
#62358=CARTESIAN_POINT('Ctrl Pts',(-21.6094419549896,26.9730005042315,14.9890256402511));
#62359=CARTESIAN_POINT('Ctrl Pts',(-21.5092584273983,26.9142225502201,14.9831746611682));
#62360=CARTESIAN_POINT('Ctrl Pts',(-21.411879510756,26.8511387495641,14.9773236820852));
#62361=CARTESIAN_POINT('Ctrl Pts',(-21.3144918388121,26.7880492770675,14.9714721769429));
#62362=CARTESIAN_POINT('Ctrl Pts',(-21.2199096260556,26.7206534131034,14.9656206718006));
#62363=CARTESIAN_POINT('Ctrl Pts',(-21.1285256308694,26.6492407242857,14.9597691666583));
#62364=CARTESIAN_POINT('Ctrl Pts',(-21.0371112890475,26.5778043208684,14.9539157183585));
#62365=CARTESIAN_POINT('Ctrl Pts',(-20.948897602183,26.5023486946252,14.9480622700587));
#62366=CARTESIAN_POINT('Ctrl Pts',(-20.8642439131024,26.4232034015927,14.942208821759));
#62367=CARTESIAN_POINT('Ctrl Pts',(-20.7794939543955,26.3439681031763,14.9363487168174));
#62368=CARTESIAN_POINT('Ctrl Pts',(-20.6983123762814,26.2610350454604,14.9304886118759));
#62369=CARTESIAN_POINT('Ctrl Pts',(-20.6210213976272,26.1747703851698,14.9246285069343));
#62370=CARTESIAN_POINT('Ctrl Pts',(-20.5436783683362,26.0884476310296,14.9187644555789));
#62371=CARTESIAN_POINT('Ctrl Pts',(-20.4702314169168,25.9987891258121,14.9129004042234));
#62372=CARTESIAN_POINT('Ctrl Pts',(-20.4009611453028,25.9061924213351,14.907036352868));
#62373=CARTESIAN_POINT('Ctrl Pts',(-20.3315887831363,25.8134592477999,14.9011636590714));
#62374=CARTESIAN_POINT('Ctrl Pts',(-20.2664056180206,25.7177795728769,14.8952909652749));
#62375=CARTESIAN_POINT('Ctrl Pts',(-20.2056478470824,25.6195781473654,14.8894182714783));
#62376=CARTESIAN_POINT('Ctrl Pts',(-20.189013385753,25.5926922397697,14.887810426155));
#62377=CARTESIAN_POINT('Ctrl Pts',(-20.1727103673945,25.565617437524,14.8862025808317));
#62378=CARTESIAN_POINT('Ctrl Pts',(-20.1567430162745,25.5383627320492,14.8845947355083));
#62379=CARTESIAN_POINT('Ctrl Pts',(-20.0984258223128,25.4388209900542,14.8787224385396));
#62380=CARTESIAN_POINT('Ctrl Pts',(-20.0443944282895,25.3365443877004,14.8728501415709));
#62381=CARTESIAN_POINT('Ctrl Pts',(-19.9949153643375,25.2319381819903,14.8669778446022));
#62382=CARTESIAN_POINT('Ctrl Pts',(-19.9455004213229,25.1274675376154,14.861113157664));
#62383=CARTESIAN_POINT('Ctrl Pts',(-19.900626251599,25.0206736637924,14.8552484707258));
#62384=CARTESIAN_POINT('Ctrl Pts',(-19.8605149992077,24.9119889016868,14.8493837837876));
#62385=CARTESIAN_POINT('Ctrl Pts',(-19.8204449987283,24.8034159150548,14.8435251283128));
#62386=CARTESIAN_POINT('Ctrl Pts',(-19.7851283147536,24.6929562936523,14.8376664728379));
#62387=CARTESIAN_POINT('Ctrl Pts',(-19.7547399244643,24.5810643711485,14.8318078173631));
#62388=CARTESIAN_POINT('Ctrl Pts',(-19.7231645368848,24.464801851599,14.8257203176452));
#62389=CARTESIAN_POINT('Ctrl Pts',(-19.6969104931754,24.3469932670035,14.8196328179273));
#62390=CARTESIAN_POINT('Ctrl Pts',(-19.6761179199509,24.2281684631287,14.8135453182094));
#62391=CARTESIAN_POINT('Ctrl Pts',(-19.6561301675324,24.1139430262197,14.807693448126));
#62392=CARTESIAN_POINT('Ctrl Pts',(-19.64118902936,23.9987790222625,14.8018415780426));
#62393=CARTESIAN_POINT('Ctrl Pts',(-19.6313671875367,23.8831589139519,14.7959897079592));
#62394=CARTESIAN_POINT('Ctrl Pts',(-19.6215468411782,23.7675564098539,14.7901387288762));
#62395=CARTESIAN_POINT('Ctrl Pts',(-19.6168442763347,23.6514983512697,14.7842877497932));
#62396=CARTESIAN_POINT('Ctrl Pts',(-19.6172803036318,23.5354723662843,14.7784367707102));
#62397=CARTESIAN_POINT('Ctrl Pts',(-19.6177163701318,23.419435949446,14.7725852655679));
#62398=CARTESIAN_POINT('Ctrl Pts',(-19.6232919456499,23.3034320253436,14.7667337604256));
#62399=CARTESIAN_POINT('Ctrl Pts',(-19.6339757154914,23.1879475512251,14.7608822552833));
#62400=CARTESIAN_POINT('Ctrl Pts',(-19.6446630331804,23.0724247272265,14.7550288069835));
#62401=CARTESIAN_POINT('Ctrl Pts',(-19.6604618801582,22.9574221076206,14.7491753586837));
#62402=CARTESIAN_POINT('Ctrl Pts',(-19.6812892354332,22.8434201525652,14.7433219103839));
#62403=CARTESIAN_POINT('Ctrl Pts',(-19.7021402759336,22.7292885525323,14.7374618054423));
#62404=CARTESIAN_POINT('Ctrl Pts',(-19.7280311643595,22.6161602953029,14.7316017005008));
#62405=CARTESIAN_POINT('Ctrl Pts',(-19.7588280198721,22.5045043922483,14.7257415955592));
#62406=CARTESIAN_POINT('Ctrl Pts',(-19.7896456151393,22.3927732959314,14.7198775442038));
#62407=CARTESIAN_POINT('Ctrl Pts',(-19.8253756290119,22.2825169204275,14.7140134928483));
#62408=CARTESIAN_POINT('Ctrl Pts',(-19.8658352717163,22.1741862344625,14.7081494414929));
#62409=CARTESIAN_POINT('Ctrl Pts',(-19.9063545438576,22.065695890691,14.7022767476963));
#62410=CARTESIAN_POINT('Ctrl Pts',(-19.9516171956521,21.9591372797747,14.6964040538998));
#62411=CARTESIAN_POINT('Ctrl Pts',(-20.001393551686,21.8549387141325,14.6905313601032));
#62412=CARTESIAN_POINT('Ctrl Pts',(-20.0150214853107,21.8264108898903,14.6889235147799));
#62413=CARTESIAN_POINT('Ctrl Pts',(-20.0289874981503,21.7980598086145,14.6873156694567));
#62414=CARTESIAN_POINT('Ctrl Pts',(-20.0432863089673,21.7698938844963,14.6857078241334));
#62415=CARTESIAN_POINT('Ctrl Pts',(-20.0955095310659,21.6670241193339,14.6798355271647));
#62416=CARTESIAN_POINT('Ctrl Pts',(-20.1523502936252,21.5662817616051,14.673963230196));
#62417=CARTESIAN_POINT('Ctrl Pts',(-20.2136117179652,21.4681101061724,14.6680909332273));
#62418=CARTESIAN_POINT('Ctrl Pts',(-20.2747937523648,21.3700656734081,14.6622262462891));
#62419=CARTESIAN_POINT('Ctrl Pts',(-20.3403848391395,21.2745856653942,14.6563615593509));
#62420=CARTESIAN_POINT('Ctrl Pts',(-20.4101413206848,21.1820906743683,14.6504968724127));
#62421=CARTESIAN_POINT('Ctrl Pts',(-20.4798260620554,21.0896908086508,14.6446382169378));
#62422=CARTESIAN_POINT('Ctrl Pts',(-20.553667429991,21.0002701817873,14.638779561463));
#62423=CARTESIAN_POINT('Ctrl Pts',(-20.6313777685368,20.9142215916248,14.6329209059882));
#62424=CARTESIAN_POINT('Ctrl Pts',(-20.7121235413526,20.8248118677399,14.6268334062703));
#62425=CARTESIAN_POINT('Ctrl Pts',(-20.7970464565817,20.739043366036,14.6207459065524));
#62426=CARTESIAN_POINT('Ctrl Pts',(-20.8857764904659,20.6573203814839,14.6146584068345));
#62427=CARTESIAN_POINT('Ctrl Pts',(-20.9710720395167,20.5787606590055,14.6088065367511));
#62428=CARTESIAN_POINT('Ctrl Pts',(-21.0598851297139,20.5039394024876,14.6029546666677));
#62429=CARTESIAN_POINT('Ctrl Pts',(-21.1518491448553,20.4331785521423,14.5971027965843));
#62430=CARTESIAN_POINT('Ctrl Pts',(-21.2437991576393,20.3624284757797,14.5912518175013));
#62431=CARTESIAN_POINT('Ctrl Pts',(-21.338898813923,20.2957378283611,14.5854008384184));
#62432=CARTESIAN_POINT('Ctrl Pts',(-21.4367491130422,20.2333877018667,14.5795498593354));
#62433=CARTESIAN_POINT('Ctrl Pts',(-21.5346082098449,20.171031969496,14.5736983541931));
#62434=CARTESIAN_POINT('Ctrl Pts',(-21.6352180924672,20.1130177559952,14.5678468490508));
#62435=CARTESIAN_POINT('Ctrl Pts',(-21.738152148686,20.0595819368225,14.5619953439085));
#62436=CARTESIAN_POINT('Ctrl Pts',(-21.8411203870648,20.0061283727773,14.5561418956087));
#62437=CARTESIAN_POINT('Ctrl Pts',(-21.9464139670337,19.9572564166125,14.5502884473089));
#62438=CARTESIAN_POINT('Ctrl Pts',(-22.0535837930351,19.9131559304585,14.5444349990091));
#62439=CARTESIAN_POINT('Ctrl Pts',(-22.1608754943995,19.8690052924756,14.5385748940676));
#62440=CARTESIAN_POINT('Ctrl Pts',(-22.2700473180871,19.8296371124323,14.5327147891261));
#62441=CARTESIAN_POINT('Ctrl Pts',(-22.380632308693,19.7951922746615,14.5268546841845));
#62442=CARTESIAN_POINT('Ctrl Pts',(-22.4912917713688,19.7607242404483,14.5209906328291));
#62443=CARTESIAN_POINT('Ctrl Pts',(-22.6033658971897,19.7311862555468,14.5151265814737));
#62444=CARTESIAN_POINT('Ctrl Pts',(-22.7163764729788,19.7066683035679,14.5092625301182));
#62445=CARTESIAN_POINT('Ctrl Pts',(-22.8295536037973,19.6821142170221,14.5033898363217));
#62446=CARTESIAN_POINT('Ctrl Pts',(-22.9436695331424,19.6625949988642,14.4975171425251));
#62447=CARTESIAN_POINT('Ctrl Pts',(-23.0582397652918,19.6481489403352,14.4916444487286));
#62448=CARTESIAN_POINT('Ctrl Pts',(-23.0896071783288,19.6441938511629,14.4900366034052));
#62449=CARTESIAN_POINT('Ctrl Pts',(-23.1210086406907,19.6406187307726,14.4884287580819));
#62450=CARTESIAN_POINT('Ctrl Pts',(-23.1524342186442,19.6374236841975,14.4868209127585));
#62451=CARTESIAN_POINT('Ctrl Pts',(-23.2672091434939,19.6257544881341,14.4809486157898));
#62452=CARTESIAN_POINT('Ctrl Pts',(-23.3826902211459,19.6191200602394,14.4750763188211));
#62453=CARTESIAN_POINT('Ctrl Pts',(-23.498398078922,19.6175943828427,14.4692040218524));
#62454=CARTESIAN_POINT('Ctrl Pts',(-23.6139559885034,19.6160706826028,14.4633393349142));
#62455=CARTESIAN_POINT('Ctrl Pts',(-23.7297396842375,19.6196425723934,14.457474647976));
#62456=CARTESIAN_POINT('Ctrl Pts',(-23.8452636075533,19.6283324069185,14.4516099610378));
#62457=CARTESIAN_POINT('Ctrl Pts',(-23.9606687217458,19.6370133044928,14.445751305563));
#62458=CARTESIAN_POINT('Ctrl Pts',(-24.0758141851743,19.6508016466365,14.4398926500882));
#62459=CARTESIAN_POINT('Ctrl Pts',(-24.1902140401816,19.6696677474568,14.4340339946133));
#62460=CARTESIAN_POINT('Ctrl Pts',(-24.3090824542876,19.6892707747923,14.4279464948954));
#62461=CARTESIAN_POINT('Ctrl Pts',(-24.4271453696354,19.7143563370762,14.4218589951775));
#62462=CARTESIAN_POINT('Ctrl Pts',(-24.543862632555,19.7448316656838,14.4157714954596));
#62463=CARTESIAN_POINT('Ctrl Pts',(-24.6560621053677,19.7741273818275,14.4099196253762));
#62464=CARTESIAN_POINT('Ctrl Pts',(-24.7670177241516,19.8084032636923,14.4040677552928));
#62465=CARTESIAN_POINT('Ctrl Pts',(-24.8762604636056,19.8475248932487,14.3982158852094));
#62466=CARTESIAN_POINT('Ctrl Pts',(-24.9854865698592,19.8866405661813,14.3923649061264));
#62467=CARTESIAN_POINT('Ctrl Pts',(-25.0929999262666,19.9306003804714,14.3865139270435));
#62468=CARTESIAN_POINT('Ctrl Pts',(-25.1983483686548,19.9792205922973,14.3806629479605));
#62469=CARTESIAN_POINT('Ctrl Pts',(-25.3037062828822,20.0278451755482,14.3748114428182));
#62470=CARTESIAN_POINT('Ctrl Pts',(-25.4068985207907,20.0811308160618,14.3689599376759));
#62471=CARTESIAN_POINT('Ctrl Pts',(-25.5074951930912,20.1388466390442,14.3631084325335));
#62472=CARTESIAN_POINT('Ctrl Pts',(-25.6081252713571,20.1965816281951,14.3572549842337));
#62473=CARTESIAN_POINT('Ctrl Pts',(-25.7061577117494,20.2587495195285,14.3514015359339));
#62474=CARTESIAN_POINT('Ctrl Pts',(-25.801190024885,20.325075109947,14.3455480876341));
#62475=CARTESIAN_POINT('Ctrl Pts',(-25.8963304103959,20.3914761269636,14.3396879826926));
#62476=CARTESIAN_POINT('Ctrl Pts',(-25.9884635196207,20.4620440436949,14.333827877751));
#62477=CARTESIAN_POINT('Ctrl Pts',(-26.0772184150144,20.5364621566787,14.3279677728095));
#62478=CARTESIAN_POINT('Ctrl Pts',(-26.1660330812752,20.6109303856041,14.322103721454));
#62479=CARTESIAN_POINT('Ctrl Pts',(-26.2514646997343,20.6892536950217,14.3162396700985));
#62480=CARTESIAN_POINT('Ctrl Pts',(-26.333179071175,20.7710783961184,14.3103756187431));
#62481=CARTESIAN_POINT('Ctrl Pts',(-26.4150138732873,20.8530236904906,14.3045029249465));
#62482=CARTESIAN_POINT('Ctrl Pts',(-26.4931202165505,20.9384803716216,14.2986302311499));
#62483=CARTESIAN_POINT('Ctrl Pts',(-26.5672039954244,21.0270615231702,14.2927575373534));
#62484=CARTESIAN_POINT('Ctrl Pts',(-26.5874868948088,21.0513135606813,14.2911496920301));
#62485=CARTESIAN_POINT('Ctrl Pts',(-26.6074685251853,21.0757996336955,14.2895418467069));
#62486=CARTESIAN_POINT('Ctrl Pts',(-26.6271434285838,21.1005114415711,14.2879340013836));
#62487=CARTESIAN_POINT('Ctrl Pts',(-26.6988772707787,21.1906096184512,14.2820718672549));
#62488=CARTESIAN_POINT('Ctrl Pts',(-26.7667760253801,21.2840191197142,14.2762097331261));
#62489=CARTESIAN_POINT('Ctrl Pts',(-26.8305176023576,21.3803792482544,14.2703475989974));
#62490=CARTESIAN_POINT('Ctrl Pts',(-26.8941790376487,21.4766182241096,14.2644928352748));
#62491=CARTESIAN_POINT('Ctrl Pts',(-26.9536934585065,21.5758001113278,14.2586380715523));
#62492=CARTESIAN_POINT('Ctrl Pts',(-27.0087785654401,21.6775308027921,14.2527833078297));
#62493=CARTESIAN_POINT('Ctrl Pts',(-27.0638078451477,21.779158393026,14.2469344777476));
#62494=CARTESIAN_POINT('Ctrl Pts',(-27.1144165399632,21.8833292898244,14.2410856476655));
#62495=CARTESIAN_POINT('Ctrl Pts',(-27.1603656938681,21.9896206224028,14.2352368175834));
#62496=CARTESIAN_POINT('Ctrl Pts',(-27.2062794802941,22.0958301415819,14.2293924893986));
#62497=CARTESIAN_POINT('Ctrl Pts',(-27.247540694878,22.2041564717086,14.2235481612138));
#62498=CARTESIAN_POINT('Ctrl Pts',(-27.2839567194601,22.314153005661,14.2177038330291));
#62499=CARTESIAN_POINT('Ctrl Pts',(-27.3203565777141,22.424100708362,14.211862099343));
#62500=CARTESIAN_POINT('Ctrl Pts',(-27.3519153914313,22.5357167483884,14.2060203656569));
#62501=CARTESIAN_POINT('Ctrl Pts',(-27.3784892419353,22.6485360073016,14.2001786319708));
#62502=CARTESIAN_POINT('Ctrl Pts',(-27.4050558725687,22.7613246142606,14.1943384854299));
#62503=CARTESIAN_POINT('Ctrl Pts',(-27.4266401422533,22.8753153859449,14.1884983388891));
#62504=CARTESIAN_POINT('Ctrl Pts',(-27.4431486424174,22.9900303694084,14.1826581923483));
#62505=CARTESIAN_POINT('Ctrl Pts',(-27.4596610348749,23.1047723998102,14.1768166688462));
#62506=CARTESIAN_POINT('Ctrl Pts',(-27.4710952060826,23.2202385729897,14.1709751453442));
#62507=CARTESIAN_POINT('Ctrl Pts',(-27.4774093433978,23.3359434644799,14.1651336218421));
#62508=CARTESIAN_POINT('Ctrl Pts',(-27.4813618919935,23.4083728690927,14.1614769219063));
#62509=CARTESIAN_POINT('Ctrl Pts',(-27.4833091581058,23.480895697148,14.1578202219705));
#62510=CARTESIAN_POINT('Ctrl Pts',(-27.483251278234,23.5533925502411,14.1541635220347));
#62511=CARTESIAN_POINT('',(-27.4855496615812,23.551270215578,12.9041639318795));
#62512=CARTESIAN_POINT('Ctrl Pts',(-27.47973650101,23.5534176803855,14.1541621116859));
#62513=CARTESIAN_POINT('Ctrl Pts',(-27.4829303983389,23.9833541344258,14.1324571044601));
#62514=CARTESIAN_POINT('Ctrl Pts',(-27.219376369067,25.7226727502858,14.0444564601096));
#62515=CARTESIAN_POINT('Ctrl Pts',(-24.6730669936168,28.0646781337204,13.8901601786337));
#62516=CARTESIAN_POINT('Ctrl Pts',(-20.3591193447167,26.9351335953461,13.691273267259));
#62517=CARTESIAN_POINT('Ctrl Pts',(-18.9775525311725,22.6951703500683,13.492386355884));
#62518=CARTESIAN_POINT('Ctrl Pts',(-21.797909317082,19.2409551306886,13.2934994445093));
#62519=CARTESIAN_POINT('Ctrl Pts',(-26.1658556103503,19.7394668882666,13.0974255340282));
#62520=CARTESIAN_POINT('Ctrl Pts',(-27.4850767383724,22.3017466999325,12.9676472606722));
#62521=CARTESIAN_POINT('Ctrl Pts',(-27.4894316120893,23.5512575959394,12.9041646244411));
#62522=CARTESIAN_POINT('',(-27.4832508490902,23.5466144882414,11.654163534408));
#62523=CARTESIAN_POINT('Ctrl Pts',(-27.4832523980892,23.5512776836369,12.9041635220348));
#62524=CARTESIAN_POINT('Ctrl Pts',(-27.4832379908657,23.6065510591407,12.9013508886097));
#62525=CARTESIAN_POINT('Ctrl Pts',(-27.4820584429071,23.6618078252927,12.8985382551845));
#62526=CARTESIAN_POINT('Ctrl Pts',(-27.4797155131848,23.7170148688545,12.8957256217594));
#62527=CARTESIAN_POINT('Ctrl Pts',(-27.4748238771176,23.8322777224003,12.8898533247907));
#62528=CARTESIAN_POINT('Ctrl Pts',(-27.4648482421994,23.9475182605675,12.883981027822));
#62529=CARTESIAN_POINT('Ctrl Pts',(-27.449784054935,24.0622514567429,12.8781087308533));
#62530=CARTESIAN_POINT('Ctrl Pts',(-27.434739389661,24.1768359678079,12.8722440439151));
#62531=CARTESIAN_POINT('Ctrl Pts',(-27.4146193391729,24.2909140382808,12.8663793569769));
#62532=CARTESIAN_POINT('Ctrl Pts',(-27.3894713312815,24.4040019146487,12.8605146700387));
#62533=CARTESIAN_POINT('Ctrl Pts',(-27.364349186542,24.5169734872153,12.8546560145639));
#62534=CARTESIAN_POINT('Ctrl Pts',(-27.3342094588585,24.6289564901327,12.8487973590891));
#62535=CARTESIAN_POINT('Ctrl Pts',(-27.2991511371522,24.7394742292743,12.8429387036143));
#62536=CARTESIAN_POINT('Ctrl Pts',(-27.2627234065209,24.8543088886497,12.8368512038964));
#62537=CARTESIAN_POINT('Ctrl Pts',(-27.220985058488,24.9675610308767,12.8307637041785));
#62538=CARTESIAN_POINT('Ctrl Pts',(-27.1741052772868,25.0787093607415,12.8246762044606));
#62539=CARTESIAN_POINT('Ctrl Pts',(-27.1290400778058,25.185555457907,12.8188243343772));
#62540=CARTESIAN_POINT('Ctrl Pts',(-27.0792242401555,25.2904571630241,12.8129724642938));
#62541=CARTESIAN_POINT('Ctrl Pts',(-27.0248579799646,25.3929695416687,12.8071205942104));
#62542=CARTESIAN_POINT('Ctrl Pts',(-26.9704999975312,25.4954663118716,12.8012696151274));
#62543=CARTESIAN_POINT('Ctrl Pts',(-26.9115931637791,25.5955741138437,12.7954186360445));
#62544=CARTESIAN_POINT('Ctrl Pts',(-26.8483840962645,25.6928717658992,12.7895676569615));
#62545=CARTESIAN_POINT('Ctrl Pts',(-26.7851693456465,25.7901781659498,12.7837161518192));
#62546=CARTESIAN_POINT('Ctrl Pts',(-26.717651817535,25.8846735671451,12.7778646466769));
#62547=CARTESIAN_POINT('Ctrl Pts',(-26.6461215837537,25.9759655840769,12.7720131415347));
#62548=CARTESIAN_POINT('Ctrl Pts',(-26.574567596339,26.0672879171002,12.7661596932349));
#62549=CARTESIAN_POINT('Ctrl Pts',(-26.4989985084209,26.1554044253891,12.7603062449352));
#62550=CARTESIAN_POINT('Ctrl Pts',(-26.4197443382093,26.2399561905277,12.7544527966354));
#62551=CARTESIAN_POINT('Ctrl Pts',(-26.3404000387964,26.3246041093836,12.7485926916939));
#62552=CARTESIAN_POINT('Ctrl Pts',(-26.2573625753744,26.4056788918726,12.7427325867523));
#62553=CARTESIAN_POINT('Ctrl Pts',(-26.1709985190359,26.4828587906101,12.7368724818108));
#62554=CARTESIAN_POINT('Ctrl Pts',(-26.0845763019109,26.5600906651786,12.7310084304554));
#62555=CARTESIAN_POINT('Ctrl Pts',(-25.9948233504204,26.6334221722495,12.7251443791));
#62556=CARTESIAN_POINT('Ctrl Pts',(-25.9021375771657,26.7025732217395,12.7192803277445));
#62557=CARTESIAN_POINT('Ctrl Pts',(-25.8093152035831,26.7718261860726,12.713407633948));
#62558=CARTESIAN_POINT('Ctrl Pts',(-25.7135517222237,26.8368861649056,12.7075349401514));
#62559=CARTESIAN_POINT('Ctrl Pts',(-25.6152721875023,26.8975175079287,12.7016622463549));
#62560=CARTESIAN_POINT('Ctrl Pts',(-25.5883648949098,26.914117355411,12.7000544010314));
#62561=CARTESIAN_POINT('Ctrl Pts',(-25.5612691343649,26.930385517104,12.698446555708));
#62562=CARTESIAN_POINT('Ctrl Pts',(-25.5339939027177,26.946317780315,12.6968387103846));
#62563=CARTESIAN_POINT('Ctrl Pts',(-25.4343771934553,27.0045068234994,12.6909664134159));
#62564=CARTESIAN_POINT('Ctrl Pts',(-25.3320311415903,27.0584065507417,12.6850941164472));
#62565=CARTESIAN_POINT('Ctrl Pts',(-25.2273613467932,27.1077509536639,12.6792218194784));
#62566=CARTESIAN_POINT('Ctrl Pts',(-25.1228271957375,27.1570314101588,12.6733571325402));
#62567=CARTESIAN_POINT('Ctrl Pts',(-25.0159756607799,27.2017681073074,12.667492445602));
#62568=CARTESIAN_POINT('Ctrl Pts',(-24.90723936861,27.2417394576412,12.6616277586638));
#62569=CARTESIAN_POINT('Ctrl Pts',(-24.7986149049096,27.2816696999434,12.655769103189));
#62570=CARTESIAN_POINT('Ctrl Pts',(-24.6881099251499,27.3168442017248,12.6499104477142));
#62571=CARTESIAN_POINT('Ctrl Pts',(-24.5761789878059,27.3470885706416,12.6440517922394));
#62572=CARTESIAN_POINT('Ctrl Pts',(-24.4598759294618,27.3785143112472,12.6379642925215));
#62573=CARTESIAN_POINT('Ctrl Pts',(-24.3420336555078,27.4046167227236,12.6318767928036));
#62574=CARTESIAN_POINT('Ctrl Pts',(-24.2231821916042,27.4252563604424,12.6257892930856));
#62575=CARTESIAN_POINT('Ctrl Pts',(-24.1089311265996,27.4450970970496,12.6199374230022));
#62576=CARTESIAN_POINT('Ctrl Pts',(-23.9937479899243,27.4598900157267,12.6140855529188));
#62577=CARTESIAN_POINT('Ctrl Pts',(-23.8781153374098,27.4695630553231,12.6082336828354));
#62578=CARTESIAN_POINT('Ctrl Pts',(-23.7625002910182,27.4792346221113,12.6023827037525));
#62579=CARTESIAN_POINT('Ctrl Pts',(-23.6464362767046,27.4837878253591,12.5965317246695));
#62580=CARTESIAN_POINT('Ctrl Pts',(-23.530410948932,27.4832024819978,12.5906807455865));
#62581=CARTESIAN_POINT('Ctrl Pts',(-23.4143751893657,27.4826170860086,12.5848292404442));
#62582=CARTESIAN_POINT('Ctrl Pts',(-23.2983785366571,27.476892227073,12.5789777353019));
#62583=CARTESIAN_POINT('Ctrl Pts',(-23.1829079073513,27.4660598465357,12.5731262301596));
#62584=CARTESIAN_POINT('Ctrl Pts',(-23.0673989327634,27.4552238688007,12.5672727818599));
#62585=CARTESIAN_POINT('Ctrl Pts',(-22.9524167402783,27.4392770354723,12.5614193335601));
#62586=CARTESIAN_POINT('Ctrl Pts',(-22.8384416828144,27.4183029857882,12.5555658852603));
#62587=CARTESIAN_POINT('Ctrl Pts',(-22.7243370109608,27.3973050840553,12.5497057803188));
#62588=CARTESIAN_POINT('Ctrl Pts',(-22.6112421669724,27.3712686297945,12.5438456753772));
#62589=CARTESIAN_POINT('Ctrl Pts',(-22.4996259895379,27.3403281073149,12.5379855704357));
#62590=CARTESIAN_POINT('Ctrl Pts',(-22.3879346455937,27.30936674833,12.5321215190802));
#62591=CARTESIAN_POINT('Ctrl Pts',(-22.2777243431423,27.2734948726586,12.5262574677248));
#62592=CARTESIAN_POINT('Ctrl Pts',(-22.1694458152998,27.2328958502848,12.5203934163693));
#62593=CARTESIAN_POINT('Ctrl Pts',(-22.0610077065216,27.1922369930563,12.5145207225728));
#62594=CARTESIAN_POINT('Ctrl Pts',(-21.9545074333599,27.1468372460926,12.5086480287762));
#62595=CARTESIAN_POINT('Ctrl Pts',(-21.8503730123046,27.0969268358219,12.5027753349796));
#62596=CARTESIAN_POINT('Ctrl Pts',(-21.8218627497758,27.083262200389,12.5011674896563));
#62597=CARTESIAN_POINT('Ctrl Pts',(-21.7935296651487,27.0692597134755,12.499559644333));
#62598=CARTESIAN_POINT('Ctrl Pts',(-21.765382165811,27.0549246671431,12.4979517990096));
#62599=CARTESIAN_POINT('Ctrl Pts',(-21.6625796930614,27.0025691028966,12.4920795020409));
#62600=CARTESIAN_POINT('Ctrl Pts',(-21.5619105683994,26.9455987398214,12.4862072050722));
#62601=CARTESIAN_POINT('Ctrl Pts',(-21.4638178329529,26.88421102692,12.4803349081035));
#62602=CARTESIAN_POINT('Ctrl Pts',(-21.3658522179012,26.8229028676193,12.4744702211653));
#62603=CARTESIAN_POINT('Ctrl Pts',(-21.2704566995842,26.75718895981,12.4686055342271));
#62604=CARTESIAN_POINT('Ctrl Pts',(-21.1780515563226,26.6873135021642,12.4627408472889));
#62605=CARTESIAN_POINT('Ctrl Pts',(-21.0857414459664,26.6175099070524,12.456882191814));
#62606=CARTESIAN_POINT('Ctrl Pts',(-20.9964159212524,26.5435535228665,12.4510235363392));
#62607=CARTESIAN_POINT('Ctrl Pts',(-20.9104674095115,26.4657325108234,12.4451648808644));
#62608=CARTESIAN_POINT('Ctrl Pts',(-20.8211616731997,26.3848717415061,12.4390773811465));
#62609=CARTESIAN_POINT('Ctrl Pts',(-20.7355025317112,26.2998385192045,12.4329898814286));
#62610=CARTESIAN_POINT('Ctrl Pts',(-20.6538938034904,26.2110033876666,12.4269023817107));
#62611=CARTESIAN_POINT('Ctrl Pts',(-20.5754439148086,26.1256068089902,12.4210505116273));
#62612=CARTESIAN_POINT('Ctrl Pts',(-20.5007370157935,26.0366975031954,12.4151986415439));
#62613=CARTESIAN_POINT('Ctrl Pts',(-20.4300945745843,25.9446425004928,12.4093467714605));
#62614=CARTESIAN_POINT('Ctrl Pts',(-20.359462889329,25.8526015140015,12.4034957923775));
#62615=CARTESIAN_POINT('Ctrl Pts',(-20.2928946830025,25.7574161107881,12.3976448132945));
#62616=CARTESIAN_POINT('Ctrl Pts',(-20.2306705338695,25.65948565293,12.3917938342115));
#62617=CARTESIAN_POINT('Ctrl Pts',(-20.1684407901866,25.5615463901813,12.3859423290692));
#62618=CARTESIAN_POINT('Ctrl Pts',(-20.1105561018261,25.4608619310883,12.3800908239269));
#62619=CARTESIAN_POINT('Ctrl Pts',(-20.0572527950333,25.3578591923609,12.3742393187846));
#62620=CARTESIAN_POINT('Ctrl Pts',(-20.0039317873726,25.2548222486663,12.3683858704849));
#62621=CARTESIAN_POINT('Ctrl Pts',(-19.9551953763324,25.1494658614805,12.3625324221851));
#62622=CARTESIAN_POINT('Ctrl Pts',(-19.9112328459345,25.042239370327,12.3566789738853));
#62623=CARTESIAN_POINT('Ctrl Pts',(-19.8672203205933,24.9348909393693,12.3508188689438));
#62624=CARTESIAN_POINT('Ctrl Pts',(-19.8279926688025,24.825668542297,12.3449587640022));
#62625=CARTESIAN_POINT('Ctrl Pts',(-19.7936901738434,24.7150393154355,12.3390986590607));
#62626=CARTESIAN_POINT('Ctrl Pts',(-19.7593645783008,24.6043355867136,12.3332346077052));
#62627=CARTESIAN_POINT('Ctrl Pts',(-19.729970848549,24.4922235406083,12.3273705563498));
#62628=CARTESIAN_POINT('Ctrl Pts',(-19.7055983527011,24.3791815057026,12.3215065049943));
#62629=CARTESIAN_POINT('Ctrl Pts',(-19.6811899366595,24.2659728694028,12.3156338111977));
#62630=CARTESIAN_POINT('Ctrl Pts',(-19.6618175929974,24.1518319148381,12.3097611174012));
#62631=CARTESIAN_POINT('Ctrl Pts',(-19.6475189894155,24.0372431866074,12.3038884236046));
#62632=CARTESIAN_POINT('Ctrl Pts',(-19.6436042709413,24.0058707096541,12.3022805782813));
#62633=CARTESIAN_POINT('Ctrl Pts',(-19.6400695647533,23.9744646723945,12.300672732958));
#62634=CARTESIAN_POINT('Ctrl Pts',(-19.6369149631006,23.9430350086886,12.2990648876347));
#62635=CARTESIAN_POINT('Ctrl Pts',(-19.6253934831084,23.8282451615342,12.293192590666));
#62636=CARTESIAN_POINT('Ctrl Pts',(-19.6189076758795,23.7127556415175,12.2873202936973));
#62637=CARTESIAN_POINT('Ctrl Pts',(-19.6175309067666,23.5970459161294,12.2814479967286));
#62638=CARTESIAN_POINT('Ctrl Pts',(-19.6161559218371,23.4814861413559,12.2755833097904));
#62639=CARTESIAN_POINT('Ctrl Pts',(-19.6198768132877,23.3657071382451,12.2697186228522));
#62640=CARTESIAN_POINT('Ctrl Pts',(-19.6287153109279,23.2501944937346,12.263853935914));
#62641=CARTESIAN_POINT('Ctrl Pts',(-19.6375447187264,23.1348006467478,12.2579952804392));
#62642=CARTESIAN_POINT('Ctrl Pts',(-19.6514812327148,23.0196730231942,12.2521366249644));
#62643=CARTESIAN_POINT('Ctrl Pts',(-19.6704945416348,22.9052975421252,12.2462779694896));
#62644=CARTESIAN_POINT('Ctrl Pts',(-19.6902505271479,22.786454454025,12.2401904697717));
#62645=CARTESIAN_POINT('Ctrl Pts',(-19.7154880064553,22.6684239196124,12.2341029700538));
#62646=CARTESIAN_POINT('Ctrl Pts',(-19.746113515873,22.5517459727239,12.2280154703359));
#62647=CARTESIAN_POINT('Ctrl Pts',(-19.7755535997588,22.439584294132,12.2221636002525));
#62648=CARTESIAN_POINT('Ctrl Pts',(-19.8099722444983,22.3286728776249,12.2163117301691));
#62649=CARTESIAN_POINT('Ctrl Pts',(-19.8492344285741,22.2194805751301,12.2104598600857));
#62650=CARTESIAN_POINT('Ctrl Pts',(-19.8884906346254,22.1103048981562,12.2046088810027));
#62651=CARTESIAN_POINT('Ctrl Pts',(-19.9325887738469,22.0028482036436,12.1987579019198));
#62652=CARTESIAN_POINT('Ctrl Pts',(-19.9813445206688,21.8975624189269,12.1929069228368));
#62653=CARTESIAN_POINT('Ctrl Pts',(-20.0301046511016,21.7922671680048,12.1870554176945));
#62654=CARTESIAN_POINT('Ctrl Pts',(-20.0835230478802,21.6891435900266,12.1812039125522));
#62655=CARTESIAN_POINT('Ctrl Pts',(-20.1413682831677,21.5886212768077,12.1753524074099));
#62656=CARTESIAN_POINT('Ctrl Pts',(-20.1992327275986,21.4880655823168,12.1694989591101));
#62657=CARTESIAN_POINT('Ctrl Pts',(-20.261526727583,21.3901132283489,12.1636455108104));
#62658=CARTESIAN_POINT('Ctrl Pts',(-20.3279745622788,21.2951663497889,12.1577920625106));
#62659=CARTESIAN_POINT('Ctrl Pts',(-20.3944979625915,21.2001114960107,12.1519319575691));
#62660=CARTESIAN_POINT('Ctrl Pts',(-20.4651843890375,21.1080692785043,12.1460718526275));
#62661=CARTESIAN_POINT('Ctrl Pts',(-20.5397166610491,21.019410226935,12.140211747686));
#62662=CARTESIAN_POINT('Ctrl Pts',(-20.614299125881,20.9306914690434,12.1343476963305));
#62663=CARTESIAN_POINT('Ctrl Pts',(-20.6927323142933,20.845360717341,12.1284836449751));
#62664=CARTESIAN_POINT('Ctrl Pts',(-20.7746621076773,20.7637517155979,12.1226195936196));
#62665=CARTESIAN_POINT('Ctrl Pts',(-20.8567126492219,20.6820224384769,12.1167468998231));
#62666=CARTESIAN_POINT('Ctrl Pts',(-20.9422697763807,20.6040261359993,12.1108742060265));
#62667=CARTESIAN_POINT('Ctrl Pts',(-21.0309461946421,20.5300564155307,12.10500151223));
#62668=CARTESIAN_POINT('Ctrl Pts',(-21.0552243145874,20.5098047434282,12.1033936669066));
#62669=CARTESIAN_POINT('Ctrl Pts',(-21.0797360821321,20.4898546412696,12.1017858215832));
#62670=CARTESIAN_POINT('Ctrl Pts',(-21.1044731896175,20.4702115563383,12.1001779762598));
#62671=CARTESIAN_POINT('Ctrl Pts',(-21.1948199656351,20.3984695632366,12.0943056792911));
#62672=CARTESIAN_POINT('Ctrl Pts',(-21.2884773827769,20.3305859632771,12.0884333823224));
#62673=CARTESIAN_POINT('Ctrl Pts',(-21.3850817140814,20.2668816524669,12.0825610853537));
#62674=CARTESIAN_POINT('Ctrl Pts',(-21.4815608538448,20.2032598973842,12.0766963984155));
#62675=CARTESIAN_POINT('Ctrl Pts',(-21.5809789712995,20.1438068863899,12.0708317114773));
#62676=CARTESIAN_POINT('Ctrl Pts',(-21.682939279891,20.0888033814625,12.0649670245391));
#62677=CARTESIAN_POINT('Ctrl Pts',(-21.7847947286877,20.0338564441966,12.0591083690643));
#62678=CARTESIAN_POINT('Ctrl Pts',(-21.8891868066446,19.9833501061082,12.0532497135895));
#62679=CARTESIAN_POINT('Ctrl Pts',(-21.9956903173906,19.937521525674,12.0473910581146));
#62680=CARTESIAN_POINT('Ctrl Pts',(-22.1063539490735,19.8899028405228,12.0413035583967));
#62681=CARTESIAN_POINT('Ctrl Pts',(-22.2192969454787,19.8473350477852,12.0352160586788));
#62682=CARTESIAN_POINT('Ctrl Pts',(-22.3340144459951,19.8100314260783,12.0291285589609));
#62683=CARTESIAN_POINT('Ctrl Pts',(-22.444291561465,19.7741717204544,12.0232766888775));
#62684=CARTESIAN_POINT('Ctrl Pts',(-22.5562079336631,19.7431763812675,12.0174248187941));
#62685=CARTESIAN_POINT('Ctrl Pts',(-22.6692961247427,19.7171852469924,12.0115729487107));
#62686=CARTESIAN_POINT('Ctrl Pts',(-22.7823670971168,19.6911980701039,12.0057219696278));
#62687=CARTESIAN_POINT('Ctrl Pts',(-22.8966091308473,19.6702136757237,11.9998709905448));
#62688=CARTESIAN_POINT('Ctrl Pts',(-23.0115423761006,19.6543212735403,11.9940200114618));
#62689=CARTESIAN_POINT('Ctrl Pts',(-23.1264859549587,19.6384274424771,11.9881685063195));
#62690=CARTESIAN_POINT('Ctrl Pts',(-23.24212045937,19.627626570338,11.9823170011772));
#62691=CARTESIAN_POINT('Ctrl Pts',(-23.3579593699759,19.6219561655889,11.9764654960349));
#62692=CARTESIAN_POINT('Ctrl Pts',(-23.4738367481622,19.6162838778217,11.9706120477352));
#62693=CARTESIAN_POINT('Ctrl Pts',(-23.5899182548459,19.6157454653782,11.9647585994354));
#62694=CARTESIAN_POINT('Ctrl Pts',(-23.7057165283975,19.6203263306404,11.9589051511356));
#62695=CARTESIAN_POINT('Ctrl Pts',(-23.8216464897311,19.6249124053412,11.9530450461941));
#62696=CARTESIAN_POINT('Ctrl Pts',(-23.9372921617307,19.6346293613958,11.9471849412525));
#62697=CARTESIAN_POINT('Ctrl Pts',(-24.052170362029,19.6494106364629,11.941324836311));
#62698=CARTESIAN_POINT('Ctrl Pts',(-24.1671259256053,19.6642018657936,11.9354607849556));
#62699=CARTESIAN_POINT('Ctrl Pts',(-24.2813125820686,19.6840641344538,11.9295967336001));
#62700=CARTESIAN_POINT('Ctrl Pts',(-24.3942581310656,19.7088799191728,11.9237326822447));
#62701=CARTESIAN_POINT('Ctrl Pts',(-24.5073701392558,19.7337322774047,11.9178599884481));
#62702=CARTESIAN_POINT('Ctrl Pts',(-24.619236991425,19.763552615995,11.9119872946515));
#62703=CARTESIAN_POINT('Ctrl Pts',(-24.7294023216681,19.798173804801,11.9061146008549));
#62704=CARTESIAN_POINT('Ctrl Pts',(-24.7595637462479,19.8076525071543,11.9045067555316));
#62705=CARTESIAN_POINT('Ctrl Pts',(-24.7895977514064,19.8174907924924,11.9028989102083));
#62706=CARTESIAN_POINT('Ctrl Pts',(-24.8194952636113,19.8276846159302,11.9012910648849));
#62707=CARTESIAN_POINT('Ctrl Pts',(-24.928689268622,19.8649152858239,11.8954187679162));
#62708=CARTESIAN_POINT('Ctrl Pts',(-25.0364266846208,19.9070168787045,11.8895464709475));
#62709=CARTESIAN_POINT('Ctrl Pts',(-25.1422409265707,19.953856842872,11.8836741739788));
#62710=CARTESIAN_POINT('Ctrl Pts',(-25.2479180416664,20.0006361061659,11.8778094870406));
#62711=CARTESIAN_POINT('Ctrl Pts',(-25.3516765644506,20.0521413636079,11.8719448001024));
#62712=CARTESIAN_POINT('Ctrl Pts',(-25.4530658052064,20.1081905557638,11.8660801131642));
#62713=CARTESIAN_POINT('Ctrl Pts',(-25.5543507734753,20.1641821048344,11.8602214576893));
#62714=CARTESIAN_POINT('Ctrl Pts',(-25.653270946747,20.2247080946832,11.8543628022145));
#62715=CARTESIAN_POINT('Ctrl Pts',(-25.7493969629523,20.2895389946802,11.8485041467397));
#62716=CARTESIAN_POINT('Ctrl Pts',(-25.849277746017,20.3569022467331,11.8424166470218));
#62717=CARTESIAN_POINT('Ctrl Pts',(-25.9461412218104,20.4289133880428,11.8363291473039));
#62718=CARTESIAN_POINT('Ctrl Pts',(-26.039535056891,20.5052629570404,11.830241647586));
#62719=CARTESIAN_POINT('Ctrl Pts',(-26.1293138847856,20.5786572534516,11.8243897775026));
#62720=CARTESIAN_POINT('Ctrl Pts',(-26.2158863273361,20.6560600803264,11.8185379074192));
#62721=CARTESIAN_POINT('Ctrl Pts',(-26.2988820661146,20.7371537629853,11.8126860373358));
#62722=CARTESIAN_POINT('Ctrl Pts',(-26.3818651680374,20.8182350983937,11.8068350582528));
#62723=CARTESIAN_POINT('Ctrl Pts',(-26.4612723534058,20.9030058833983,11.8009840791698));
#62724=CARTESIAN_POINT('Ctrl Pts',(-26.5367691894349,20.9911106339017,11.7951331000868));
#62725=CARTESIAN_POINT('Ctrl Pts',(-26.6122728133561,21.0792233058699,11.7892815949445));
#62726=CARTESIAN_POINT('Ctrl Pts',(-26.6838651200353,21.1706702253029,11.7834300898022));
#62727=CARTESIAN_POINT('Ctrl Pts',(-26.7512515686327,21.2650623502172,11.7775785846599));
#62728=CARTESIAN_POINT('Ctrl Pts',(-26.8186603948028,21.3594858207015,11.7717251363601));
#62729=CARTESIAN_POINT('Ctrl Pts',(-26.8818603456322,21.4568561051683,11.7658716880603));
#62730=CARTESIAN_POINT('Ctrl Pts',(-26.9406002627201,21.5567552874704,11.7600182397605));
#62731=CARTESIAN_POINT('Ctrl Pts',(-26.9994069798488,21.6567680768355,11.754158134819));
#62732=CARTESIAN_POINT('Ctrl Pts',(-27.0537433299704,21.7593151476993,11.7482980298774));
#62733=CARTESIAN_POINT('Ctrl Pts',(-27.1034041325464,21.8639540108619,11.7424379249359));
#62734=CARTESIAN_POINT('Ctrl Pts',(-27.1530983785649,21.9686633417498,11.7365738735804));
#62735=CARTESIAN_POINT('Ctrl Pts',(-27.1981106472213,22.0754668899169,11.7307098222249));
#62736=CARTESIAN_POINT('Ctrl Pts',(-27.2382845685065,22.1839038589733,11.7248457708695));
#62737=CARTESIAN_POINT('Ctrl Pts',(-27.2785176981321,22.2925006424758,11.7189730770729));
#62738=CARTESIAN_POINT('Ctrl Pts',(-27.3138981229128,22.4027352593177,11.7131003832763));
#62739=CARTESIAN_POINT('Ctrl Pts',(-27.3443197671237,22.5141334202786,11.7072276894797));
#62740=CARTESIAN_POINT('Ctrl Pts',(-27.3526487044162,22.5446323732845,11.7056198441565));
#62741=CARTESIAN_POINT('Ctrl Pts',(-27.3606062429117,22.5752184960405,11.7040119988332));
#62742=CARTESIAN_POINT('Ctrl Pts',(-27.3681908810109,22.6058819683997,11.70240415351));
#62743=CARTESIAN_POINT('Ctrl Pts',(-27.4061182065104,22.7592160473512,11.6943640503263));
#62744=CARTESIAN_POINT('Ctrl Pts',(-27.4348232418154,22.9149150857894,11.6863239471426));
#62745=CARTESIAN_POINT('Ctrl Pts',(-27.4540696900141,23.0720260221748,11.6782838439589));
#62746=CARTESIAN_POINT('Ctrl Pts',(-27.4722823314705,23.2206978770397,11.6706756081408));
#62747=CARTESIAN_POINT('Ctrl Pts',(-27.4820254920152,23.370634264891,11.6630673723228));
#62748=CARTESIAN_POINT('Ctrl Pts',(-27.4831437745779,23.5210040847501,11.6554591365047));
#62749=CARTESIAN_POINT('Ctrl Pts',(-27.4832072518091,23.5295395480976,11.6550272691391));
#62750=CARTESIAN_POINT('Ctrl Pts',(-27.4832429513159,23.5380764008163,11.6545954017735));
#62751=CARTESIAN_POINT('Ctrl Pts',(-27.4832508490902,23.5466144882414,11.654163534408));
#62752=CARTESIAN_POINT('',(-27.4768104533793,23.5508499486531,10.4041635220348));
#62753=CARTESIAN_POINT('Ctrl Pts',(-27.4828563374966,23.5466150977616,11.6541635220348));
#62754=CARTESIAN_POINT('Ctrl Pts',(-27.4737453654797,24.5392918724205,11.6039480954016));
#62755=CARTESIAN_POINT('Ctrl Pts',(-26.5880752141214,26.8569989905617,11.4874370316434));
#62756=CARTESIAN_POINT('Ctrl Pts',(-22.6892863486302,28.1218483213199,11.3046303307602));
#62757=CARTESIAN_POINT('Ctrl Pts',(-19.2387035696249,25.2970485643742,11.1057434193855));
#62758=CARTESIAN_POINT('Ctrl Pts',(-19.7500687276925,20.8670913572745,10.9068565080105));
#62759=CARTESIAN_POINT('Ctrl Pts',(-23.7534805991851,18.9027317749154,10.7079695966357));
#62760=CARTESIAN_POINT('Ctrl Pts',(-26.96905917351,20.8458290658098,10.5404052679771));
#62761=CARTESIAN_POINT('Ctrl Pts',(-27.4758729437841,22.8568035385642,10.4391365764434));
#62762=CARTESIAN_POINT('Ctrl Pts',(-27.4768104533793,23.5508499486531,10.4041635220348));
#62763=CARTESIAN_POINT('',(-27.4833612647152,23.5536820313857,9.15416357631301));
#62764=CARTESIAN_POINT('Ctrl Pts',(-27.4768104533793,23.5508499486531,10.4041635220348));
#62765=CARTESIAN_POINT('Ctrl Pts',(-27.4776501061447,24.172452106559,10.3728409393185));
#62766=CARTESIAN_POINT('Ctrl Pts',(-27.0450601870018,26.1085981990694,10.2752227194772));
#62767=CARTESIAN_POINT('Ctrl Pts',(-24.0088794396662,28.1795518513951,10.1113088625109));
#62768=CARTESIAN_POINT('Ctrl Pts',(-19.9034526288354,26.4384355765543,9.91242195113609));
#62769=CARTESIAN_POINT('Ctrl Pts',(-19.1491257310881,22.0433239610247,9.71353503976112));
#62770=CARTESIAN_POINT('Ctrl Pts',(-22.4390612090823,19.032951935469,9.51464812838629));
#62771=CARTESIAN_POINT('Ctrl Pts',(-26.4806567721111,20.1023081666841,9.32819125204667));
#62772=CARTESIAN_POINT('Ctrl Pts',(-27.4753001046528,22.4903580385635,9.20803001283191));
#62773=CARTESIAN_POINT('Ctrl Pts',(-27.4850558365148,23.5536670379096,9.15416441074218));
#62774=CARTESIAN_POINT('',(-27.484942279697,23.5480589111923,7.90416291743633));
#62775=CARTESIAN_POINT('Ctrl Pts',(-27.4832510356148,23.5536830066866,9.15416352203477));
#62776=CARTESIAN_POINT('Ctrl Pts',(-27.4831009438724,23.7257613921932,9.14544221748674));
#62777=CARTESIAN_POINT('Ctrl Pts',(-27.4716543896873,23.89736605375,9.1367209129387));
#62778=CARTESIAN_POINT('Ctrl Pts',(-27.4491156108634,24.0673170246647,9.12799960839067));
#62779=CARTESIAN_POINT('Ctrl Pts',(-27.4395317717813,24.1395828190911,9.12429117413927));
#62780=CARTESIAN_POINT('Ctrl Pts',(-27.4279428892403,24.2115500617344,9.12058273988788));
#62781=CARTESIAN_POINT('Ctrl Pts',(-27.4143669509749,24.2831295709763,9.11687430563648));
#62782=CARTESIAN_POINT('Ctrl Pts',(-27.3928694844651,24.3964755565454,9.11100200866777));
#62783=CARTESIAN_POINT('Ctrl Pts',(-27.3663446125213,24.5090647482891,9.10512971169906));
#62784=CARTESIAN_POINT('Ctrl Pts',(-27.3348579229357,24.6204165530412,9.09925741473035));
#62785=CARTESIAN_POINT('Ctrl Pts',(-27.3034120375993,24.7316240546977,9.09339272779215));
#62786=CARTESIAN_POINT('Ctrl Pts',(-27.2670172332676,24.8415969641444,9.08752804085395));
#62787=CARTESIAN_POINT('Ctrl Pts',(-27.2257903493916,24.9498634600155,9.08166335391575));
#62788=CARTESIAN_POINT('Ctrl Pts',(-27.1846058647847,25.0580186105734,9.07580469844092));
#62789=CARTESIAN_POINT('Ctrl Pts',(-27.1385993314306,25.1644704542212,9.0699460429661));
#62790=CARTESIAN_POINT('Ctrl Pts',(-27.0879375884499,25.2687616062142,9.06408738749128));
#62791=CARTESIAN_POINT('Ctrl Pts',(-27.035296953166,25.3771264624625,9.05799988777337));
#62792=CARTESIAN_POINT('Ctrl Pts',(-26.9776301449224,25.4831579513821,9.05191238805547));
#62793=CARTESIAN_POINT('Ctrl Pts',(-26.9151799068011,25.5863646995907,9.04582488833756));
#62794=CARTESIAN_POINT('Ctrl Pts',(-26.8551469380786,25.6855766109227,9.03997301825416));
#62795=CARTESIAN_POINT('Ctrl Pts',(-26.7906941935824,25.7821780039988,9.03412114817076));
#62796=CARTESIAN_POINT('Ctrl Pts',(-26.722084086784,25.8757575491338,9.02826927808736));
#62797=CARTESIAN_POINT('Ctrl Pts',(-26.6534844264982,25.9693228459322,9.02241829900439));
#62798=CARTESIAN_POINT('Ctrl Pts',(-26.5807289068674,26.0598668763354,9.01656731992142));
#62799=CARTESIAN_POINT('Ctrl Pts',(-26.5041224235725,26.1470085198177,9.01071634083845));
#62800=CARTESIAN_POINT('Ctrl Pts',(-26.4275090526175,26.2341579981722,9.00486483569616));
#62801=CARTESIAN_POINT('Ctrl Pts',(-26.3470443026595,26.3179041710017,8.99901333055387));
#62802=CARTESIAN_POINT('Ctrl Pts',(-26.2630719060061,26.3979006915549,8.99316182541158));
#62803=CARTESIAN_POINT('Ctrl Pts',(-26.1790716239477,26.4779237772112,8.98730837711181));
#62804=CARTESIAN_POINT('Ctrl Pts',(-26.0915616781838,26.5541944496501,8.98145492881204));
#62805=CARTESIAN_POINT('Ctrl Pts',(-26.000920491604,26.626405250639,8.97560148051227));
#62806=CARTESIAN_POINT('Ctrl Pts',(-25.9101762263126,26.698698170989,8.96974137557073));
#62807=CARTESIAN_POINT('Ctrl Pts',(-25.8162939362699,26.7669217468522,8.96388127062918));
#62808=CARTESIAN_POINT('Ctrl Pts',(-25.719682841778,26.8308105832595,8.95802116568764));
#62809=CARTESIAN_POINT('Ctrl Pts',(-25.6230066857607,26.8947424447994,8.9521571143322));
#62810=CARTESIAN_POINT('Ctrl Pts',(-25.5235984198017,26.9543335422019,8.94629306297675));
#62811=CARTESIAN_POINT('Ctrl Pts',(-25.4218922566159,27.0093642298177,8.94042901162131));
#62812=CARTESIAN_POINT('Ctrl Pts',(-25.320036198848,27.064476021682,8.93455631782474));
#62813=CARTESIAN_POINT('Ctrl Pts',(-25.2158758552907,27.1150138098997,8.92868362402817));
#62814=CARTESIAN_POINT('Ctrl Pts',(-25.1098658733538,27.1608058444868,8.9228109302316));
#62815=CARTESIAN_POINT('Ctrl Pts',(-25.0808421136298,27.1733429375496,8.92120308490826));
#62816=CARTESIAN_POINT('Ctrl Pts',(-25.0516797978485,27.1855245902506,8.91959523958493));
#62817=CARTESIAN_POINT('Ctrl Pts',(-25.0223884372128,27.1973479342965,8.91798739426159));
#62818=CARTESIAN_POINT('Ctrl Pts',(-24.9154082658157,27.2405300653095,8.91211509729288));
#62819=CARTESIAN_POINT('Ctrl Pts',(-24.8063472719977,27.2790734766344,8.90624280032417));
#62820=CARTESIAN_POINT('Ctrl Pts',(-24.6956452398352,27.3127735674012,8.90037050335546));
#62821=CARTESIAN_POINT('Ctrl Pts',(-24.5850866687145,27.3464299855268,8.89450581641726));
#62822=CARTESIAN_POINT('Ctrl Pts',(-24.4728916802176,27.3752554456401,8.88864112947905));
#62823=CARTESIAN_POINT('Ctrl Pts',(-24.3595203822524,27.3990932072812,8.88277644254084));
#62824=CARTESIAN_POINT('Ctrl Pts',(-24.24626567957,27.4229064532767,8.87691778706602));
#62825=CARTESIAN_POINT('Ctrl Pts',(-24.1318374758005,27.4417421191626,8.8710591315912));
#62826=CARTESIAN_POINT('Ctrl Pts',(-24.0167107600212,27.4554933336456,8.86520047611637));
#62827=CARTESIAN_POINT('Ctrl Pts',(-23.8970870933214,27.4697816826782,8.85911297639847));
#62828=CARTESIAN_POINT('Ctrl Pts',(-23.7767096681456,27.4785801441099,8.85302547668056));
#62829=CARTESIAN_POINT('Ctrl Pts',(-23.6561230980913,27.4818273336242,8.84693797696266));
#62830=CARTESIAN_POINT('Ctrl Pts',(-23.540204087913,27.4849488337563,8.84108610687926));
#62831=CARTESIAN_POINT('Ctrl Pts',(-23.4240922743701,27.4829408065889,8.83523423679586));
#62832=CARTESIAN_POINT('Ctrl Pts',(-23.3082755616338,27.4758016838461,8.82938236671245));
#62833=CARTESIAN_POINT('Ctrl Pts',(-23.1924764830452,27.4686636480996,8.82353138762948));
#62834=CARTESIAN_POINT('Ctrl Pts',(-23.0769728284111,27.4563960955909,8.81768040854651));
#62835=CARTESIAN_POINT('Ctrl Pts',(-22.9622500498651,27.439049528371,8.81182942946354));
#62836=CARTESIAN_POINT('Ctrl Pts',(-22.8475169566374,27.4217014015278,8.80597792432124));
#62837=CARTESIAN_POINT('Ctrl Pts',(-22.7335652878266,27.3992734139972,8.80012641917894));
#62838=CARTESIAN_POINT('Ctrl Pts',(-22.6208722326499,27.3718675384353,8.79427491403665));
#62839=CARTESIAN_POINT('Ctrl Pts',(-22.5081417545628,27.3444525619786,8.78842146573687));
#62840=CARTESIAN_POINT('Ctrl Pts',(-22.3966711226563,27.3120565081404,8.78256801743709));
#62841=CARTESIAN_POINT('Ctrl Pts',(-22.2869235603145,27.2748315562381,8.77671456913731));
#62842=CARTESIAN_POINT('Ctrl Pts',(-22.1770511911632,27.2375642714824,8.77085446419577));
#62843=CARTESIAN_POINT('Ctrl Pts',(-22.0689061943966,27.1954572606458,8.76499435925422));
#62844=CARTESIAN_POINT('Ctrl Pts',(-21.9629330521766,27.1487113504031,8.75913425431268));
#62845=CARTESIAN_POINT('Ctrl Pts',(-21.8568885436779,27.1019339597155,8.75327020295723));
#62846=CARTESIAN_POINT('Ctrl Pts',(-21.7530191716326,27.0505116320596,8.74740615160178));
#62847=CARTESIAN_POINT('Ctrl Pts',(-21.6517444379905,26.994690950093,8.74154210024633));
#62848=CARTESIAN_POINT('Ctrl Pts',(-21.5503204456075,26.938787999584,8.73566940644975));
#62849=CARTESIAN_POINT('Ctrl Pts',(-21.4514990750814,26.8784739719018,8.72979671265317));
#62850=CARTESIAN_POINT('Ctrl Pts',(-21.3556705787541,26.814038531393,8.7239240188566));
#62851=CARTESIAN_POINT('Ctrl Pts',(-21.3294343394752,26.7963971856553,8.7223161735333));
#62852=CARTESIAN_POINT('Ctrl Pts',(-21.3034222427136,26.7784471397982,8.72070832821001));
#62853=CARTESIAN_POINT('Ctrl Pts',(-21.2776418428209,26.7601948453221,8.71910048288671));
#62854=CARTESIAN_POINT('Ctrl Pts',(-21.1834846736277,26.6935324046191,8.713228185918));
#62855=CARTESIAN_POINT('Ctrl Pts',(-21.092105364407,26.62261190846,8.7073558889493));
#62856=CARTESIAN_POINT('Ctrl Pts',(-21.0039137712404,26.5476927591233,8.70148359198059));
#62857=CARTESIAN_POINT('Ctrl Pts',(-20.9158364673745,26.4728706990543,8.69561890504239));
#62858=CARTESIAN_POINT('Ctrl Pts',(-20.8309389765748,26.394060555986,8.68975421810419));
#62859=CARTESIAN_POINT('Ctrl Pts',(-20.7496018750497,26.3115647015578,8.68388953116599));
#62860=CARTESIAN_POINT('Ctrl Pts',(-20.6683484236418,26.2291536889516,8.67803087569118));
#62861=CARTESIAN_POINT('Ctrl Pts',(-20.5906483668093,26.1430647971276,8.67217222021636));
#62862=CARTESIAN_POINT('Ctrl Pts',(-20.5168483688969,26.0536398739016,8.66631356474154));
#62863=CARTESIAN_POINT('Ctrl Pts',(-20.4401656780638,25.9607219344098,8.66022606502364));
#62864=CARTESIAN_POINT('Ctrl Pts',(-20.3676942833698,25.8642023282843,8.65413856530574));
#62865=CARTESIAN_POINT('Ctrl Pts',(-20.2997802152074,25.7645060672571,8.64805106558783));
#62866=CARTESIAN_POINT('Ctrl Pts',(-20.2344949056159,25.6686687622276,8.64219919550444));
#62867=CARTESIAN_POINT('Ctrl Pts',(-20.1734209350139,25.5698965215311,8.63634732542104));
#62868=CARTESIAN_POINT('Ctrl Pts',(-20.1168233557066,25.4685989794134,8.63049545533765));
#62869=CARTESIAN_POINT('Ctrl Pts',(-20.0602343938953,25.3673168607675,8.62464447625468));
#62870=CARTESIAN_POINT('Ctrl Pts',(-20.0081206697716,25.2635105659856,8.61879349717172));
#62871=CARTESIAN_POINT('Ctrl Pts',(-19.9607021025708,25.1576158125924,8.61294251808875));
#62872=CARTESIAN_POINT('Ctrl Pts',(-19.9132792719845,25.0517115382418,8.60709101294646));
#62873=CARTESIAN_POINT('Ctrl Pts',(-19.87055260645,24.943718809312,8.60123950780416));
#62874=CARTESIAN_POINT('Ctrl Pts',(-19.832694255662,24.8340942136413,8.59538800266187));
#62875=CARTESIAN_POINT('Ctrl Pts',(-19.79482333294,24.7244332140289,8.58953455436211));
#62876=CARTESIAN_POINT('Ctrl Pts',(-19.7618240744621,24.6131396606585,8.58368110606234));
#62877=CARTESIAN_POINT('Ctrl Pts',(-19.7338188410917,24.500685530508,8.57782765776258));
#62878=CARTESIAN_POINT('Ctrl Pts',(-19.7057817596898,24.3881035155926,8.57196755282104));
#62879=CARTESIAN_POINT('Ctrl Pts',(-19.6827501390441,24.2743586909295,8.56610744787951));
#62880=CARTESIAN_POINT('Ctrl Pts',(-19.6647952817554,24.1599335621504,8.56024734293797));
#62881=CARTESIAN_POINT('Ctrl Pts',(-19.646828332994,24.0454313752086,8.55438329158253));
#62882=CARTESIAN_POINT('Ctrl Pts',(-19.6339450011017,23.9302483817159,8.54851924022708));
#62883=CARTESIAN_POINT('Ctrl Pts',(-19.6261645905391,23.8148708040808,8.54265518887164));
#62884=CARTESIAN_POINT('Ctrl Pts',(-19.6183727132044,23.6993231829279,8.53678249507507));
#62885=CARTESIAN_POINT('Ctrl Pts',(-19.6156987765524,23.5835808169997,8.5309098012785));
#62886=CARTESIAN_POINT('Ctrl Pts',(-19.6181100290429,23.4681286079983,8.52503710748194));
#62887=CARTESIAN_POINT('Ctrl Pts',(-19.6187701896395,23.4365197244525,8.52342926215857));
#62888=CARTESIAN_POINT('Ctrl Pts',(-19.6198112233587,23.404932550266,8.5218214168352));
#62889=CARTESIAN_POINT('Ctrl Pts',(-19.6212317858923,23.3733769283509,8.52021357151183));
#62890=CARTESIAN_POINT('Ctrl Pts',(-19.62642007418,23.2581270468949,8.51434127454312));
#62891=CARTESIAN_POINT('Ctrl Pts',(-19.6366922870426,23.1429125661555,8.50846897757441));
#62892=CARTESIAN_POINT('Ctrl Pts',(-19.6520517295779,23.0282185228594,8.5025966806057));
#62893=CARTESIAN_POINT('Ctrl Pts',(-19.6673912674956,22.9136731139346,8.4967319936675));
#62894=CARTESIAN_POINT('Ctrl Pts',(-19.6878048703177,22.7996472071662,8.49086730672929));
#62895=CARTESIAN_POINT('Ctrl Pts',(-19.7132438652852,22.6866244323931,8.48500261979109));
#62896=CARTESIAN_POINT('Ctrl Pts',(-19.7386566978389,22.5737178944686,8.47914396431627));
#62897=CARTESIAN_POINT('Ctrl Pts',(-19.769084552294,22.4618128373866,8.47328530884145));
#62898=CARTESIAN_POINT('Ctrl Pts',(-19.8044272131219,22.351385698913,8.46742665336663));
#62899=CARTESIAN_POINT('Ctrl Pts',(-19.8411503894112,22.2366451791477,8.46133915364872));
#62900=CARTESIAN_POINT('Ctrl Pts',(-19.8831800923618,22.1235008399813,8.45525165393082));
#62901=CARTESIAN_POINT('Ctrl Pts',(-19.930345796569,22.0124735394475,8.44916415421291));
#62902=CARTESIAN_POINT('Ctrl Pts',(-19.9756858517975,21.9057437869148,8.44331228412951));
#62903=CARTESIAN_POINT('Ctrl Pts',(-20.0257715249008,21.8009706473841,8.43746041404611));
#62904=CARTESIAN_POINT('Ctrl Pts',(-20.0804014557224,21.6985985384824,8.43160854396271));
#62905=CARTESIAN_POINT('Ctrl Pts',(-20.1350230686402,21.596242016665,8.42575756487973));
#62906=CARTESIAN_POINT('Ctrl Pts',(-20.1941873689816,21.496286163192,8.41990658579677));
#62907=CARTESIAN_POINT('Ctrl Pts',(-20.2576466559519,21.3991515235992,8.4140556067138));
#62908=CARTESIAN_POINT('Ctrl Pts',(-20.3211116485229,21.3020081506675,8.4082041015715));
#62909=CARTESIAN_POINT('Ctrl Pts',(-20.388872169267,21.2076868419514,8.4023525964292));
#62910=CARTESIAN_POINT('Ctrl Pts',(-20.4606371373831,21.1165792349602,8.3965010912869));
#62911=CARTESIAN_POINT('Ctrl Pts',(-20.5324259370829,21.0254413731161,8.39064764298712));
#62912=CARTESIAN_POINT('Ctrl Pts',(-20.6082215726991,20.9375196596236,8.38479419468735));
#62913=CARTESIAN_POINT('Ctrl Pts',(-20.6876931033152,20.853172162295,8.37894074638757));
#62914=CARTESIAN_POINT('Ctrl Pts',(-20.7672550103185,20.7687287435463,8.37308064144603));
#62915=CARTESIAN_POINT('Ctrl Pts',(-20.8505008724078,20.6878679549511,8.3672205365045));
#62916=CARTESIAN_POINT('Ctrl Pts',(-20.9370632915779,20.6109105993324,8.36136043156296));
#62917=CARTESIAN_POINT('Ctrl Pts',(-21.0236840051196,20.5339014177513,8.3554963802075));
#62918=CARTESIAN_POINT('Ctrl Pts',(-21.1136254030629,20.4608011635339,8.34963232885205));
#62919=CARTESIAN_POINT('Ctrl Pts',(-21.2064888532168,20.3918889016715,8.3437682774966));
#62920=CARTESIAN_POINT('Ctrl Pts',(-21.2994891655588,20.3228750768914,8.33789558370003));
#62921=CARTESIAN_POINT('Ctrl Pts',(-21.3954197838516,20.2580617936708,8.33202288990346));
#62922=CARTESIAN_POINT('Ctrl Pts',(-21.4938550485616,20.1976836075159,8.32615019610689));
#62923=CARTESIAN_POINT('Ctrl Pts',(-21.5208049774182,20.1811530701505,8.32454235078357));
#62924=CARTESIAN_POINT('Ctrl Pts',(-21.5479425198958,20.1649547025624,8.32293450546025));
#62925=CARTESIAN_POINT('Ctrl Pts',(-21.5752586683316,20.149092694274,8.32132666013692));
#62926=CARTESIAN_POINT('Ctrl Pts',(-21.6750248170582,20.0911602415446,8.31545436316821));
#62927=CARTESIAN_POINT('Ctrl Pts',(-21.7775092593236,20.0375241154475,8.3095820661995));
#62928=CARTESIAN_POINT('Ctrl Pts',(-21.882305712137,19.9884492795298,8.30370976923078));
#62929=CARTESIAN_POINT('Ctrl Pts',(-21.9869663570703,19.939438040702,8.29784508229258));
#62930=CARTESIAN_POINT('Ctrl Pts',(-22.0939326833089,19.8949765107511,8.29198039535437));
#62931=CARTESIAN_POINT('Ctrl Pts',(-22.2027714952651,19.8552851628986,8.28611570841616));
#62932=CARTESIAN_POINT('Ctrl Pts',(-22.3114983733167,19.8156346351127,8.28025705294133));
#62933=CARTESIAN_POINT('Ctrl Pts',(-22.4220935206719,19.7807446722469,8.2743983974665));
#62934=CARTESIAN_POINT('Ctrl Pts',(-22.5341019315029,19.7507884961056,8.26853974199168));
#62935=CARTESIAN_POINT('Ctrl Pts',(-22.6504854895165,19.7196622053393,8.26245224227378));
#62936=CARTESIAN_POINT('Ctrl Pts',(-22.7683945566312,19.693863187768,8.25636474255587));
#62937=CARTESIAN_POINT('Ctrl Pts',(-22.8872987500339,19.6735295233556,8.25027724283797));
#62938=CARTESIAN_POINT('Ctrl Pts',(-23.0016005035302,19.6539829167066,8.24442537275457));
#62939=CARTESIAN_POINT('Ctrl Pts',(-23.1168213333218,19.6394865102733,8.23857350267116));
#62940=CARTESIAN_POINT('Ctrl Pts',(-23.2324784997017,19.6301111229449,8.23272163258776));
#62941=CARTESIAN_POINT('Ctrl Pts',(-23.3481180562263,19.6207371631044,8.22687065350478));
#62942=CARTESIAN_POINT('Ctrl Pts',(-23.4641934053245,19.6164827054232,8.22101967442181));
#62943=CARTESIAN_POINT('Ctrl Pts',(-23.5802168422007,19.6173666777574,8.21516869533883));
#62944=CARTESIAN_POINT('Ctrl Pts',(-23.6962507107003,19.6182507295693,8.20931719019653));
#62945=CARTESIAN_POINT('Ctrl Pts',(-23.812232244304,19.624274126649,8.20346568505422));
#62946=CARTESIAN_POINT('Ctrl Pts',(-23.9276746102915,19.6354036745112,8.19761417991192));
#62947=CARTESIAN_POINT('Ctrl Pts',(-24.0431553121755,19.6465369182539,8.19176073161215));
#62948=CARTESIAN_POINT('Ctrl Pts',(-24.1580960791646,19.662779644807,8.18590728331237));
#62949=CARTESIAN_POINT('Ctrl Pts',(-24.2720167752056,19.6840469788571,8.1800538350126));
#62950=CARTESIAN_POINT('Ctrl Pts',(-24.3860670238156,19.7053384984841,8.17419373007105));
#62951=CARTESIAN_POINT('Ctrl Pts',(-24.499094479465,19.7316659548117,8.1683336251295));
#62952=CARTESIAN_POINT('Ctrl Pts',(-24.6106306511595,19.7628936572595,8.16247352018795));
#62953=CARTESIAN_POINT('Ctrl Pts',(-24.7222419354847,19.7941423896104,8.1566094688325));
#62954=CARTESIAN_POINT('Ctrl Pts',(-24.8323595443267,19.8302978104149,8.15074541747705));
#62955=CARTESIAN_POINT('Ctrl Pts',(-24.9405332180278,19.8711753901806,8.1448813661216));
#62956=CARTESIAN_POINT('Ctrl Pts',(-25.0488663181304,19.9121132153389,8.13900867232502));
#62957=CARTESIAN_POINT('Ctrl Pts',(-25.1552493867321,19.9577869268456,8.13313597852844));
#62958=CARTESIAN_POINT('Ctrl Pts',(-25.2592550013274,20.0079651973878,8.12726328473186));
#62959=CARTESIAN_POINT('Ctrl Pts',(-25.2877299988013,20.0217031684819,8.12565543940858));
#62960=CARTESIAN_POINT('Ctrl Pts',(-25.3160269493838,20.0357785339095,8.12404759408529));
#62961=CARTESIAN_POINT('Ctrl Pts',(-25.3441374593362,20.0501859799871,8.122439748762));
#62962=CARTESIAN_POINT('Ctrl Pts',(-25.4468048365961,20.1028059681805,8.11656745179331));
#62963=CARTESIAN_POINT('Ctrl Pts',(-25.5473269950698,20.1600352490152,8.11069515482462));
#62964=CARTESIAN_POINT('Ctrl Pts',(-25.6452614032994,20.2216752338242,8.10482285785592));
#62965=CARTESIAN_POINT('Ctrl Pts',(-25.7430688963137,20.2832353381083,8.09895817091773));
#62966=CARTESIAN_POINT('Ctrl Pts',(-25.8382949614041,20.3491945612836,8.09309348397953));
#62967=CARTESIAN_POINT('Ctrl Pts',(-25.9305199501705,20.4193076237567,8.08722879704134));
#62968=CARTESIAN_POINT('Ctrl Pts',(-26.0226500913092,20.489348579334,8.08137014156654));
#62969=CARTESIAN_POINT('Ctrl Pts',(-26.1117849680669,20.5635346283769,8.07551148609173));
#62970=CARTESIAN_POINT('Ctrl Pts',(-26.1975328960942,20.6415766005767,8.06965283061693));
#62971=CARTESIAN_POINT('Ctrl Pts',(-26.2866302137162,20.7226669609493,8.06356533089902));
#62972=CARTESIAN_POINT('Ctrl Pts',(-26.372070209357,20.8079203747251,8.05747783118112));
#62973=CARTESIAN_POINT('Ctrl Pts',(-26.4534500196312,20.8969652600185,8.05139033146321));
#62974=CARTESIAN_POINT('Ctrl Pts',(-26.5316798511226,20.9825634734845,8.04553846137983));
#62975=CARTESIAN_POINT('Ctrl Pts',(-26.6061576641391,21.0716647685679,8.03968659129644));
#62976=CARTESIAN_POINT('Ctrl Pts',(-26.6765629362846,21.1639012888655,8.03383472121305));
#62977=CARTESIAN_POINT('Ctrl Pts',(-26.7469574885872,21.2561237653142,8.0279837421301));
#62978=CARTESIAN_POINT('Ctrl Pts',(-26.8132804821875,21.3514801893151,8.02213276304714));
#62979=CARTESIAN_POINT('Ctrl Pts',(-26.8752523676452,21.4495704779494,8.01628178396418));
#62980=CARTESIAN_POINT('Ctrl Pts',(-26.9372298249719,21.5476695858446,8.0104302788219));
#62981=CARTESIAN_POINT('Ctrl Pts',(-26.9948551756657,21.6485026975033,8.00457877367962));
#62982=CARTESIAN_POINT('Ctrl Pts',(-27.0478931930804,21.7516422893632,7.99872726853734));
#62983=CARTESIAN_POINT('Ctrl Pts',(-27.1009488232661,21.8548161316364,7.99287382023757));
#62984=CARTESIAN_POINT('Ctrl Pts',(-27.1494139021352,21.9602976096887,7.9870203719378));
#62985=CARTESIAN_POINT('Ctrl Pts',(-27.1931003028217,22.0676368982977,7.98116692363804));
#62986=CARTESIAN_POINT('Ctrl Pts',(-27.236836384432,22.175098254986,7.97530681869651));
#62987=CARTESIAN_POINT('Ctrl Pts',(-27.2757827850475,22.2844212560711,7.96944671375498));
#62988=CARTESIAN_POINT('Ctrl Pts',(-27.309800424187,22.395138405708,7.96358660881346));
#62989=CARTESIAN_POINT('Ctrl Pts',(-27.3438409720774,22.5059301164157,7.95772255745801));
#62990=CARTESIAN_POINT('Ctrl Pts',(-27.372946045726,22.6181174459967,7.95185850610257));
#62991=CARTESIAN_POINT('Ctrl Pts',(-27.3970275084582,22.7312218374328,7.94599445474712));
#62992=CARTESIAN_POINT('Ctrl Pts',(-27.4211444624592,22.8444929221638,7.94012176095057));
#62993=CARTESIAN_POINT('Ctrl Pts',(-27.4402229611217,22.9586833600148,7.93424906715401));
#62994=CARTESIAN_POINT('Ctrl Pts',(-27.454226584011,23.073308511041,7.92837637335746));
#62995=CARTESIAN_POINT('Ctrl Pts',(-27.4580605417064,23.1046909599492,7.92676852803404));
#62996=CARTESIAN_POINT('Ctrl Pts',(-27.4615144019953,23.1361059909608,7.92516068271063));
#62997=CARTESIAN_POINT('Ctrl Pts',(-27.4645880981971,23.1675436700113,7.92355283738721));
#62998=CARTESIAN_POINT('Ctrl Pts',(-27.4769435290101,23.2939146718693,7.91708973226972));
#62999=CARTESIAN_POINT('Ctrl Pts',(-27.4831806393559,23.4208935378221,7.91062662715224));
#63000=CARTESIAN_POINT('Ctrl Pts',(-27.4832519138216,23.5480479488766,7.90416352203479));
#63001=CARTESIAN_POINT('',(-27.4815060178495,23.5478800874245,6.65416403612834));
#63002=CARTESIAN_POINT('Ctrl Pts',(-27.488217119783,23.5480801490979,7.90416174611401));
#63003=CARTESIAN_POINT('Ctrl Pts',(-27.4802939371502,24.726698147767,7.84432980608009));
#63004=CARTESIAN_POINT('Ctrl Pts',(-26.2908702967356,27.2250975801982,7.71820222892116));
#63005=CARTESIAN_POINT('Ctrl Pts',(-22.0376613007461,27.9494363878388,7.52577901463738));
#63006=CARTESIAN_POINT('Ctrl Pts',(-19.0315256593045,24.6556295193558,7.32689210326248));
#63007=CARTESIAN_POINT('Ctrl Pts',(-20.1777168887306,20.3460749197242,7.12800519188759));
#63008=CARTESIAN_POINT('Ctrl Pts',(-24.4229824301708,18.9808878760331,6.92911828051277));
#63009=CARTESIAN_POINT('Ctrl Pts',(-27.1574915769292,21.2312579726243,6.77117155548725));
#63010=CARTESIAN_POINT('Ctrl Pts',(-27.4809117896271,23.0451161699384,6.67952046758692));
#63011=CARTESIAN_POINT('Ctrl Pts',(-27.4781757282195,23.5478626436939,6.65416501681149));
#63012=CARTESIAN_POINT('',(-27.4822036273482,23.5533406583821,5.40416311071642));
#63013=CARTESIAN_POINT('Ctrl Pts',(-27.4832518216526,23.5478892317737,6.6541635220348));
#63014=CARTESIAN_POINT('Ctrl Pts',(-27.4833222665197,23.6651234473433,6.64825855696148));
#63015=CARTESIAN_POINT('Ctrl Pts',(-27.4781466245375,23.782371779065,6.64235359188816));
#63016=CARTESIAN_POINT('Ctrl Pts',(-27.4677476936434,23.8991374068391,6.63644862681483));
#63017=CARTESIAN_POINT('Ctrl Pts',(-27.4573471920843,24.0159206710108,6.63054276984966));
#63018=CARTESIAN_POINT('Ctrl Pts',(-27.4417218669083,24.132220684945,6.62463691288448));
#63019=CARTESIAN_POINT('Ctrl Pts',(-27.4209463972919,24.2475458694113,6.6187310559193));
#63020=CARTESIAN_POINT('Ctrl Pts',(-27.4001631103339,24.362914448148,6.61282297671311));
#63021=CARTESIAN_POINT('Ctrl Pts',(-27.3742258936023,24.4773070712476,6.60691489750693));
#63022=CARTESIAN_POINT('Ctrl Pts',(-27.3432604098945,24.5902430296848,6.60100681830074));
#63023=CARTESIAN_POINT('Ctrl Pts',(-27.3122539242018,24.7033285287683,6.59509091609472));
#63024=CARTESIAN_POINT('Ctrl Pts',(-27.2762059788322,24.8149531213812,6.5891750138887));
#63025=CARTESIAN_POINT('Ctrl Pts',(-27.2352920947175,24.9246514617553,6.58325911168269));
#63026=CARTESIAN_POINT('Ctrl Pts',(-27.1943505456958,25.0344239773011,6.57733920929708));
#63027=CARTESIAN_POINT('Ctrl Pts',(-27.1485366593428,25.142267274952,6.57141930691147));
#63028=CARTESIAN_POINT('Ctrl Pts',(-27.098073320373,25.247737922329,6.56549940452586));
#63029=CARTESIAN_POINT('Ctrl Pts',(-27.0475167459688,25.353403435956,6.55956856460259));
#63030=CARTESIAN_POINT('Ctrl Pts',(-26.9922937422482,25.4566871835873,6.55363772467932));
#63031=CARTESIAN_POINT('Ctrl Pts',(-26.9326725741186,25.5571714778916,6.54770688475605));
#63032=CARTESIAN_POINT('Ctrl Pts',(-26.8778435210453,25.6495792397364,6.54225274242501));
#63033=CARTESIAN_POINT('Ctrl Pts',(-26.8192955474047,25.7396196142019,6.53679860009397));
#63034=CARTESIAN_POINT('Ctrl Pts',(-26.7572675138849,25.8269922849389,6.53134445776294));
#63035=CARTESIAN_POINT('Ctrl Pts',(-26.6904839554248,25.9210635867819,6.52547216079422));
#63036=CARTESIAN_POINT('Ctrl Pts',(-26.6194459199246,26.0123515511663,6.51959986382549));
#63037=CARTESIAN_POINT('Ctrl Pts',(-26.5444133369009,26.1004466561804,6.51372756685677));
#63038=CARTESIAN_POINT('Ctrl Pts',(-26.4694779901458,26.1884275969348,6.50786287991856));
#63039=CARTESIAN_POINT('Ctrl Pts',(-26.3905586558662,26.2732235949031,6.50199819298035));
#63040=CARTESIAN_POINT('Ctrl Pts',(-26.3079581952231,26.3544544633212,6.49613350604213));
#63041=CARTESIAN_POINT('Ctrl Pts',(-26.2254426839828,26.4356017908763,6.4902748505673));
#63042=CARTESIAN_POINT('Ctrl Pts',(-26.139253869513,26.5131909936536,6.48441619509246));
#63043=CARTESIAN_POINT('Ctrl Pts',(-26.0497340454763,26.5868758475273,6.47855753961762));
#63044=CARTESIAN_POINT('Ctrl Pts',(-25.9567174982651,26.6634388966939,6.47247003989972));
#63045=CARTESIAN_POINT('Ctrl Pts',(-25.8601047070134,26.7357860181436,6.46638254018182));
#63046=CARTESIAN_POINT('Ctrl Pts',(-25.7603211284155,26.8035717287276,6.46029504046392));
#63047=CARTESIAN_POINT('Ctrl Pts',(-25.6643998856275,26.8687336490942,6.4544431703805));
#63048=CARTESIAN_POINT('Ctrl Pts',(-25.5655491292688,26.9296804569246,6.44859130029709));
#63049=CARTESIAN_POINT('Ctrl Pts',(-25.4641788343479,26.9861476273004,6.44273943021368));
#63050=CARTESIAN_POINT('Ctrl Pts',(-25.3628239739761,27.042606200036,6.4368884511307));
#63051=CARTESIAN_POINT('Ctrl Pts',(-25.2589506988417,27.0945862903713,6.43103747204773));
#63052=CARTESIAN_POINT('Ctrl Pts',(-25.1529950091274,27.1418685399879,6.42518649296475));
#63053=CARTESIAN_POINT('Ctrl Pts',(-25.0470297929768,27.1891550407337,6.41933498782244));
#63054=CARTESIAN_POINT('Ctrl Pts',(-24.9389821675759,27.2317426926378,6.41348348268013));
#63055=CARTESIAN_POINT('Ctrl Pts',(-24.8293089419281,27.269459933741,6.40763197753783));
#63056=CARTESIAN_POINT('Ctrl Pts',(-24.7195992961896,27.3071896999189,6.40177852923805));
#63057=CARTESIAN_POINT('Ctrl Pts',(-24.6082633674985,27.3400457049168,6.39592508093827));
#63058=CARTESIAN_POINT('Ctrl Pts',(-24.4957732899104,27.3679061953707,6.39007163263848));
#63059=CARTESIAN_POINT('Ctrl Pts',(-24.3831552866774,27.3957983692519,6.38421152769694));
#63060=CARTESIAN_POINT('Ctrl Pts',(-24.2693809162986,27.418683590076,6.37835142275539));
#63061=CARTESIAN_POINT('Ctrl Pts',(-24.1549327757671,27.4364911762486,6.37249131781385));
#63062=CARTESIAN_POINT('Ctrl Pts',(-24.040407561576,27.454310754716,6.3666272664584));
#63063=CARTESIAN_POINT('Ctrl Pts',(-23.9252080836176,27.4670458443789,6.36076321510295));
#63064=CARTESIAN_POINT('Ctrl Pts',(-23.8098205887411,27.474677766523,6.3548991637475));
#63065=CARTESIAN_POINT('Ctrl Pts',(-23.6942630357306,27.4823209365969,6.34902646995092));
#63066=CARTESIAN_POINT('Ctrl Pts',(-23.5785173244979,27.4848459196048,6.34315377615434));
#63067=CARTESIAN_POINT('Ctrl Pts',(-23.463068314195,27.4822860910905,6.33728108235776));
#63068=CARTESIAN_POINT('Ctrl Pts',(-23.431460306402,27.4815852528641,6.33567323703452));
#63069=CARTESIAN_POINT('Ctrl Pts',(-23.3998744981043,27.4805035697687,6.33406539171128));
#63070=CARTESIAN_POINT('Ctrl Pts',(-23.368320730476,27.4790423987787,6.33245754638804));
#63071=CARTESIAN_POINT('Ctrl Pts',(-23.2530776213804,27.4737057971468,6.32658524941933));
#63072=CARTESIAN_POINT('Ctrl Pts',(-23.1378764555881,27.4632853207081,6.32071295245062));
#63073=CARTESIAN_POINT('Ctrl Pts',(-23.0232022736771,27.4477782885718,6.31484065548191));
#63074=CARTESIAN_POINT('Ctrl Pts',(-22.9086767003989,27.4322913523176,6.30897596854371));
#63075=CARTESIAN_POINT('Ctrl Pts',(-22.794677158774,27.4117310239195,6.30311128160551));
#63076=CARTESIAN_POINT('Ctrl Pts',(-22.6816872156028,27.3861465984905,6.29724659466731));
#63077=CARTESIAN_POINT('Ctrl Pts',(-22.5688134755146,27.3605884850413,6.29138793919247));
#63078=CARTESIAN_POINT('Ctrl Pts',(-22.456947669383,27.3300166426716,6.28552928371763));
#63079=CARTESIAN_POINT('Ctrl Pts',(-22.3465661056098,27.2945318999652,6.27967062824279));
#63080=CARTESIAN_POINT('Ctrl Pts',(-22.2318729407332,27.2576610919544,6.27358312852489));
#63081=CARTESIAN_POINT('Ctrl Pts',(-22.1187827842212,27.2154858158368,6.26749562880699));
#63082=CARTESIAN_POINT('Ctrl Pts',(-22.0078162742232,27.1681772671798,6.26140812908909));
#63083=CARTESIAN_POINT('Ctrl Pts',(-21.9011449591992,27.1226998966002,6.25555625900569));
#63084=CARTESIAN_POINT('Ctrl Pts',(-21.7964363627984,27.0724794300842,6.24970438892229));
#63085=CARTESIAN_POINT('Ctrl Pts',(-21.6941346431447,27.0177177995529,6.2438525188389));
#63086=CARTESIAN_POINT('Ctrl Pts',(-21.5918484998579,26.9629645069777,6.23800153975592));
#63087=CARTESIAN_POINT('Ctrl Pts',(-21.4919688690131,26.9036716202144,6.23215056067295));
#63088=CARTESIAN_POINT('Ctrl Pts',(-21.3949159770263,26.8400873810616,6.22629958158997));
#63089=CARTESIAN_POINT('Ctrl Pts',(-21.2978543590507,26.7764974250739,6.22044807644767));
#63090=CARTESIAN_POINT('Ctrl Pts',(-21.2036203309646,26.7086155762474,6.21459657130537));
#63091=CARTESIAN_POINT('Ctrl Pts',(-21.1126051553548,26.6367334191493,6.20874506616308));
#63092=CARTESIAN_POINT('Ctrl Pts',(-21.0215597555869,26.564827391552,6.20289161786333));
#63093=CARTESIAN_POINT('Ctrl Pts',(-20.9337356579938,26.4889186702892,6.19703816956359));
#63094=CARTESIAN_POINT('Ctrl Pts',(-20.849490504196,26.409338656809,6.19118472126384));
#63095=CARTESIAN_POINT('Ctrl Pts',(-20.7651495453644,26.3296681435725,6.18532461632229));
#63096=CARTESIAN_POINT('Ctrl Pts',(-20.6843959546835,26.2463182888672,6.17946451138075));
#63097=CARTESIAN_POINT('Ctrl Pts',(-20.6075500618979,26.1596569032424,6.1736044064392));
#63098=CARTESIAN_POINT('Ctrl Pts',(-20.5306524182131,26.0729371565982,6.16774035508373));
#63099=CARTESIAN_POINT('Ctrl Pts',(-20.4576679721178,25.9829017587879,6.16187630372827));
#63100=CARTESIAN_POINT('Ctrl Pts',(-20.3888752753636,25.8899497008073,6.1560122523728));
#63101=CARTESIAN_POINT('Ctrl Pts',(-20.3199811919069,25.7968606500485,6.15013955857623));
#63102=CARTESIAN_POINT('Ctrl Pts',(-20.2552914176074,25.700846701536,6.14426686477966));
#63103=CARTESIAN_POINT('Ctrl Pts',(-20.1950399599862,25.6023338163056,6.13839417098309));
#63104=CARTESIAN_POINT('Ctrl Pts',(-20.1785441187734,25.5753626362491,6.13678632565977));
#63105=CARTESIAN_POINT('Ctrl Pts',(-20.1623806885072,25.5482042702037,6.13517848033645));
#63106=CARTESIAN_POINT('Ctrl Pts',(-20.146553847114,25.5208677312162,6.13357063501314));
#63107=CARTESIAN_POINT('Ctrl Pts',(-20.0887498336375,25.4210271105404,6.12769833804444));
#63108=CARTESIAN_POINT('Ctrl Pts',(-20.0352456414679,25.3184737276152,6.12182604107573));
#63109=CARTESIAN_POINT('Ctrl Pts',(-19.9863057110786,25.2136142060826,6.11595374410703));
#63110=CARTESIAN_POINT('Ctrl Pts',(-19.9374292029522,25.1088905741617,6.11008905716881));
#63111=CARTESIAN_POINT('Ctrl Pts',(-19.8931053671678,25.0018671179666,6.1042243702306));
#63112=CARTESIAN_POINT('Ctrl Pts',(-19.8535541192753,24.8929773164581,6.09835968329238));
#63113=CARTESIAN_POINT('Ctrl Pts',(-19.8140435473655,24.7841995012945,6.09250102781758));
#63114=CARTESIAN_POINT('Ctrl Pts',(-19.779295940751,24.6735595448514,6.08664237234278));
#63115=CARTESIAN_POINT('Ctrl Pts',(-19.7494839355358,24.5615126755029,6.08078371686799));
#63116=CARTESIAN_POINT('Ctrl Pts',(-19.7185074471386,24.4450891567475,6.07469621715008));
#63117=CARTESIAN_POINT('Ctrl Pts',(-19.6928601907367,24.3271469859409,6.06860871743217));
#63118=CARTESIAN_POINT('Ctrl Pts',(-19.672679563618,24.2082167231552,6.06252121771427));
#63119=CARTESIAN_POINT('Ctrl Pts',(-19.6532800706287,24.0938899093469,6.05666934763087));
#63120=CARTESIAN_POINT('Ctrl Pts',(-19.6389319564528,23.9786505192196,6.05081747754747));
#63121=CARTESIAN_POINT('Ctrl Pts',(-19.6297054186723,23.8629813832189,6.04496560746407));
#63122=CARTESIAN_POINT('Ctrl Pts',(-19.6204802857162,23.7473298588962,6.03911462838111));
#63123=CARTESIAN_POINT('Ctrl Pts',(-19.6163752115111,23.6312491307621,6.03326364929815));
#63124=CARTESIAN_POINT('Ctrl Pts',(-19.6174084962593,23.5152269275672,6.02741267021519));
#63125=CARTESIAN_POINT('Ctrl Pts',(-19.6184418739098,23.3991942928596,6.0215611650729));
#63126=CARTESIAN_POINT('Ctrl Pts',(-19.6246145252214,23.2832206069425,6.0157096599306));
#63127=CARTESIAN_POINT('Ctrl Pts',(-19.6358926292203,23.1677926594144,6.0098581547883));
#63128=CARTESIAN_POINT('Ctrl Pts',(-19.647174478432,23.0523263807778,6.00400470648854));
#63129=CARTESIAN_POINT('Ctrl Pts',(-19.6635651113687,22.9374066120962,5.99815125818877));
#63130=CARTESIAN_POINT('Ctrl Pts',(-19.6849790348896,22.8235133797974,5.992297809889));
#63131=CARTESIAN_POINT('Ctrl Pts',(-19.7064173106914,22.709490626162,5.98643770494747));
#63132=CARTESIAN_POINT('Ctrl Pts',(-19.7328902027685,22.5964971454994,5.98057760000594));
#63133=CARTESIAN_POINT('Ctrl Pts',(-19.7642614177415,22.4850012537926,5.97471749506441));
#63134=CARTESIAN_POINT('Ctrl Pts',(-19.7956537592642,22.373430276581,5.96885344370896));
#63135=CARTESIAN_POINT('Ctrl Pts',(-19.8319508629333,22.2633592881424,5.96298939235352));
#63136=CARTESIAN_POINT('Ctrl Pts',(-19.8729676199596,22.1552383102866,5.95712534099807));
#63137=CARTESIAN_POINT('Ctrl Pts',(-19.9140448274981,22.0469579836927,5.95125264720151));
#63138=CARTESIAN_POINT('Ctrl Pts',(-19.9598554079241,21.9406337817025,5.94537995340495));
#63139=CARTESIAN_POINT('Ctrl Pts',(-20.0101674840569,21.8366928287674,5.9395072596084));
#63140=CARTESIAN_POINT('Ctrl Pts',(-20.0239420888843,21.8082355345725,5.93789941428501));
#63141=CARTESIAN_POINT('Ctrl Pts',(-20.0380538586334,21.7799567213217,5.93629156896162));
#63142=CARTESIAN_POINT('Ctrl Pts',(-20.052497468823,21.7518647759088,5.93468372363823));
#63143=CARTESIAN_POINT('Ctrl Pts',(-20.1052495383782,21.6492652015011,5.92881142666951));
#63144=CARTESIAN_POINT('Ctrl Pts',(-20.1626081360278,21.5488167759046,5.9229391297008));
#63145=CARTESIAN_POINT('Ctrl Pts',(-20.224374103766,21.4509617746426,5.91706683273209));
#63146=CARTESIAN_POINT('Ctrl Pts',(-20.2860600277152,21.353233585691,5.91120214579389));
#63147=CARTESIAN_POINT('Ctrl Pts',(-20.3521417448157,21.2580924838499,5.9053374588557));
#63148=CARTESIAN_POINT('Ctrl Pts',(-20.4223734356222,21.165957801516,5.89947277191751));
#63149=CARTESIAN_POINT('Ctrl Pts',(-20.4925328975314,21.0739178739349,5.89361411644268));
#63150=CARTESIAN_POINT('Ctrl Pts',(-20.5668335948011,20.9848785426677,5.88775546096786));
#63151=CARTESIAN_POINT('Ctrl Pts',(-20.644985853295,20.8992311195997,5.88189680549304));
#63152=CARTESIAN_POINT('Ctrl Pts',(-20.7261908078412,20.8102382327495,5.87580930577513));
#63153=CARTESIAN_POINT('Ctrl Pts',(-20.8115541056541,20.7249080223781,5.86972180605723));
#63154=CARTESIAN_POINT('Ctrl Pts',(-20.900703646702,20.6436428733402,5.86363430633932));
#63155=CARTESIAN_POINT('Ctrl Pts',(-20.9864024649988,20.5655232648779,5.85778243625592));
#63156=CARTESIAN_POINT('Ctrl Pts',(-21.0755995334561,20.4911601799772,5.85193056617253));
#63157=CARTESIAN_POINT('Ctrl Pts',(-21.1679265834877,20.4208736673663,5.84607869608913));
#63158=CARTESIAN_POINT('Ctrl Pts',(-21.2602395758866,20.350597856516,5.84022771700616));
#63159=CARTESIAN_POINT('Ctrl Pts',(-21.3556812734628,20.2843976341435,5.83437673792319));
#63160=CARTESIAN_POINT('Ctrl Pts',(-21.4538512338705,20.2225520345816,5.82852575884022));
#63161=CARTESIAN_POINT('Ctrl Pts',(-21.5520300207027,20.1607008745051,5.8226742536979));
#63162=CARTESIAN_POINT('Ctrl Pts',(-21.6529372082114,20.1032053359079,5.81682274855559));
#63163=CARTESIAN_POINT('Ctrl Pts',(-21.75614497047,20.0503000950519,5.81097124341327));
#63164=CARTESIAN_POINT('Ctrl Pts',(-21.8593870057799,19.997377285517,5.80511779511347));
#63165=CARTESIAN_POINT('Ctrl Pts',(-21.9649307672754,19.9490479932454,5.79926434681366));
#63166=CARTESIAN_POINT('Ctrl Pts',(-22.0723261880017,19.9054997660571,5.79341089851385));
#63167=CARTESIAN_POINT('Ctrl Pts',(-22.1798437406413,19.8619020150783,5.7875507935723));
#63168=CARTESIAN_POINT('Ctrl Pts',(-22.289216772189,19.8230963369197,5.78169068863074));
#63169=CARTESIAN_POINT('Ctrl Pts',(-22.399977608201,19.7892212103167,5.77583058368919));
#63170=CARTESIAN_POINT('Ctrl Pts',(-22.5108130347039,19.755323270936,5.76996653233373));
#63171=CARTESIAN_POINT('Ctrl Pts',(-22.6230377273525,19.7263625977631,5.76410248097826));
#63172=CARTESIAN_POINT('Ctrl Pts',(-22.7361730161001,19.7024267115342,5.75823842962279));
#63173=CARTESIAN_POINT('Ctrl Pts',(-22.8494750436791,19.678455548587,5.75236573582621));
#63174=CARTESIAN_POINT('Ctrl Pts',(-22.9636899395163,19.6595240199423,5.74649304202963));
#63175=CARTESIAN_POINT('Ctrl Pts',(-23.0783330171981,19.6456679223103,5.74062034823305));
#63176=CARTESIAN_POINT('Ctrl Pts',(-23.1097203741213,19.6418743545631,5.7390125029098));
#63177=CARTESIAN_POINT('Ctrl Pts',(-23.1411398239651,19.638460925838,5.73740465758655));
#63178=CARTESIAN_POINT('Ctrl Pts',(-23.1725814325873,19.6354276900315,5.73579681226331));
#63179=CARTESIAN_POINT('Ctrl Pts',(-23.2874149058908,19.6243494717635,5.72992451529461));
#63180=CARTESIAN_POINT('Ctrl Pts',(-23.4029286053266,19.618309589997,5.72405221832591));
#63181=CARTESIAN_POINT('Ctrl Pts',(-23.5186427837313,19.6173795584298,5.7181799213572));
#63182=CARTESIAN_POINT('Ctrl Pts',(-23.6342070057502,19.6164507321096,5.71231523441902));
#63183=CARTESIAN_POINT('Ctrl Pts',(-23.7499707805255,19.6206185905788,5.70645054748083));
#63184=CARTESIAN_POINT('Ctrl Pts',(-23.865448440845,19.629902988751,5.70058586054265));
#63185=CARTESIAN_POINT('Ctrl Pts',(-23.9808073396196,19.6391778385009,5.69472720506786));
#63186=CARTESIAN_POINT('Ctrl Pts',(-24.0958802996424,19.6535587285542,5.68886854959307));
#63187=CARTESIAN_POINT('Ctrl Pts',(-24.2101815225078,19.6730134718626,5.68300989411828));
#63188=CARTESIAN_POINT('Ctrl Pts',(-24.3289474518143,19.6932281345803,5.67692239440037));
#63189=CARTESIAN_POINT('Ctrl Pts',(-24.4468796707661,19.7189211131666,5.67083489468246));
#63190=CARTESIAN_POINT('Ctrl Pts',(-24.5634385103922,19.749996859694,5.66474739496456));
#63191=CARTESIAN_POINT('Ctrl Pts',(-24.6754856920217,19.7798697533038,5.65889552488117));
#63192=CARTESIAN_POINT('Ctrl Pts',(-24.7862633998641,19.8147163437034,5.65304365479778));
#63193=CARTESIAN_POINT('Ctrl Pts',(-24.8953033067715,19.8543998002581,5.64719178471439));
#63194=CARTESIAN_POINT('Ctrl Pts',(-25.0043266113616,19.8940772146456,5.64134080563143));
#63195=CARTESIAN_POINT('Ctrl Pts',(-25.1116122527678,19.9385898895416,5.63548982654847));
#63196=CARTESIAN_POINT('Ctrl Pts',(-25.2167090186601,19.9877517559681,5.62963884746552));
#63197=CARTESIAN_POINT('Ctrl Pts',(-25.3218152337632,20.0369180425195,5.62378734232322));
#63198=CARTESIAN_POINT('Ctrl Pts',(-25.4247318076668,20.0907341763954,5.61793583718093));
#63199=CARTESIAN_POINT('Ctrl Pts',(-25.5250300452443,20.1489670729335,5.61208433203863));
#63200=CARTESIAN_POINT('Ctrl Pts',(-25.6253615896828,20.2072193073487,5.60623088373887));
#63201=CARTESIAN_POINT('Ctrl Pts',(-25.7230727115568,20.2698910134365,5.60037743543911));
#63202=CARTESIAN_POINT('Ctrl Pts',(-25.8177623434703,20.336704919864,5.59452398713936));
#63203=CARTESIAN_POINT('Ctrl Pts',(-25.9125596580567,20.4035948082116,5.58866388219782));
#63204=CARTESIAN_POINT('Ctrl Pts',(-26.0043282863861,20.4746360606059,5.58280377725629));
#63205=CARTESIAN_POINT('Ctrl Pts',(-26.092698926112,20.5495100683175,5.57694367231475));
#63206=CARTESIAN_POINT('Ctrl Pts',(-26.1811290779332,20.6244344989875,5.57107962095928));
#63207=CARTESIAN_POINT('Ctrl Pts',(-26.266156382102,20.7031965442662,5.56521556960381));
#63208=CARTESIAN_POINT('Ctrl Pts',(-26.3474484645022,20.7854407996801,5.55935151824835));
#63209=CARTESIAN_POINT('Ctrl Pts',(-26.4288603552039,20.8678062667086,5.55347882445179));
#63210=CARTESIAN_POINT('Ctrl Pts',(-26.5065257610035,20.9536638811046,5.54760613065524));
#63211=CARTESIAN_POINT('Ctrl Pts',(-26.5801525719743,21.0426252176958,5.54173343685868));
#63212=CARTESIAN_POINT('Ctrl Pts',(-26.6003103611928,21.0669813435141,5.54012559153529));
#63213=CARTESIAN_POINT('Ctrl Pts',(-26.6201656806579,21.0915699509017,5.5385177462119));
#63214=CARTESIAN_POINT('Ctrl Pts',(-26.6397131152008,21.1163827112315,5.5369099008885));
#63215=CARTESIAN_POINT('Ctrl Pts',(-26.7110486478897,21.206933288174,5.53104230213154));
#63216=CARTESIAN_POINT('Ctrl Pts',(-26.778524082213,21.300780476233,5.52517470337458));
#63217=CARTESIAN_POINT('Ctrl Pts',(-26.8418188622549,21.3975611716709,5.51930710461762));
#63218=CARTESIAN_POINT('Ctrl Pts',(-26.9050336190289,21.4942195077686,5.51344692423587));
#63219=CARTESIAN_POINT('Ctrl Pts',(-26.9640780044036,21.5938036364398,5.50758674385412));
#63220=CARTESIAN_POINT('Ctrl Pts',(-27.018671442544,21.6959172710525,5.50172656347237));
#63221=CARTESIAN_POINT('Ctrl Pts',(-27.0732091005547,21.7979265723976,5.4958723706531));
#63222=CARTESIAN_POINT('Ctrl Pts',(-27.1233046598979,21.9024598788128,5.49001817783384));
#63223=CARTESIAN_POINT('Ctrl Pts',(-27.1687210445858,22.0090923773909,5.48416398501457));
#63224=CARTESIAN_POINT('Ctrl Pts',(-27.2141020393429,22.1156417844424,5.4783143539736));
#63225=CARTESIAN_POINT('Ctrl Pts',(-27.2548109499471,22.2242867513825,5.47246472293264));
#63226=CARTESIAN_POINT('Ctrl Pts',(-27.2906571616852,22.3345789719167,5.46661509189167));
#63227=CARTESIAN_POINT('Ctrl Pts',(-27.3264865824959,22.4448195298464,5.46076820090955));
#63228=CARTESIAN_POINT('Ctrl Pts',(-27.3574577056136,22.5567054147355,5.45492130992742));
#63229=CARTESIAN_POINT('Ctrl Pts',(-27.3834287131429,22.6697700719174,5.4490744189453));
#63230=CARTESIAN_POINT('Ctrl Pts',(-27.4093924142585,22.7828029206627,5.44322917286677));
#63231=CARTESIAN_POINT('Ctrl Pts',(-27.4303587085588,22.8970134785583,5.43738392678824));
#63232=CARTESIAN_POINT('Ctrl Pts',(-27.4462363456635,23.0119225944907,5.43153868070971));
#63233=CARTESIAN_POINT('Ctrl Pts',(-27.4621171030454,23.1268542923917,5.42569228592195));
#63234=CARTESIAN_POINT('Ctrl Pts',(-27.4729071469972,23.2424844130739,5.41984589113418));
#63235=CARTESIAN_POINT('Ctrl Pts',(-27.4785668570434,23.3583266052125,5.41399949634641));
#63236=CARTESIAN_POINT('Ctrl Pts',(-27.4817408223472,23.4232909047189,5.41072083824254));
#63237=CARTESIAN_POINT('Ctrl Pts',(-27.4833022499328,23.4883218102957,5.40744218013866));
#63238=CARTESIAN_POINT('Ctrl Pts',(-27.4832513250676,23.5533333307847,5.40416352203479));
#63239=CARTESIAN_POINT('',(-27.4893522825259,23.5513991534028,4.15416352203478));
#63240=CARTESIAN_POINT('Ctrl Pts',(-27.4795712903284,23.553359068946,5.40416207728037));
#63241=CARTESIAN_POINT('Ctrl Pts',(-27.4827450664922,23.9901033867319,5.38211571469144));
#63242=CARTESIAN_POINT('Ctrl Pts',(-27.213804749291,25.7363791598107,5.29377371497752));
#63243=CARTESIAN_POINT('Ctrl Pts',(-24.6498133537127,28.0703981964695,5.13913607813869));
#63244=CARTESIAN_POINT('Ctrl Pts',(-20.3417373817907,26.9186618543491,4.9402491667638));
#63245=CARTESIAN_POINT('Ctrl Pts',(-18.9820147954062,22.6716429387221,4.74136225538889));
#63246=CARTESIAN_POINT('Ctrl Pts',(-21.8201153659821,19.2319917452288,4.54247534401407));
#63247=CARTESIAN_POINT('Ctrl Pts',(-26.1778457211819,19.7520755616869,4.34674243289589));
#63248=CARTESIAN_POINT('Ctrl Pts',(-27.484577323702,22.308533202287,4.2173051589029));
#63249=CARTESIAN_POINT('Ctrl Pts',(-27.4893522825259,23.5513991534028,4.15416352203478));
#63250=CARTESIAN_POINT('',(-27.4830612926269,23.5466160075057,2.90416352203478));
#63251=CARTESIAN_POINT('Ctrl Pts',(-27.4893522825259,23.5513991534028,4.15416352203478));
#63252=CARTESIAN_POINT('Ctrl Pts',(-27.4895907974283,23.6134817936935,4.15100952177793));
#63253=CARTESIAN_POINT('Ctrl Pts',(-27.4882507228628,23.6755539139368,4.14785552152109));
#63254=CARTESIAN_POINT('Ctrl Pts',(-27.4232753800365,25.0406653481724,4.07840588413927));
#63255=CARTESIAN_POINT('Ctrl Pts',(-25.8759180657365,27.5791519665122,3.94581460988933));
#63256=CARTESIAN_POINT('Ctrl Pts',(-21.4177926524215,27.6846649077641,3.74692769851445));
#63257=CARTESIAN_POINT('Ctrl Pts',(-18.9192170653763,23.9910034157703,3.54804078713955));
#63258=CARTESIAN_POINT('Ctrl Pts',(-20.6761704248198,19.8923292308246,3.34915387576474));
#63259=CARTESIAN_POINT('Ctrl Pts',(-25.0741615585053,19.1549764186241,3.15026696438971));
#63260=CARTESIAN_POINT('Ctrl Pts',(-27.3098113051133,21.6172642433357,3.00193684647982));
#63261=CARTESIAN_POINT('Ctrl Pts',(-27.4859294268932,23.2355262183984,2.91990236569482));
#63262=CARTESIAN_POINT('Ctrl Pts',(-27.4830612926269,23.5466160075057,2.90416352203478));
#63263=CARTESIAN_POINT('',(-27.4767827643537,23.550738941023,1.65416352203481));
#63264=CARTESIAN_POINT('Ctrl Pts',(-27.4830612926269,23.5466160075057,2.90416352203478));
#63265=CARTESIAN_POINT('Ctrl Pts',(-27.4738481842906,24.5459081128646,2.85360672856985));
#63266=CARTESIAN_POINT('Ctrl Pts',(-26.5783054564929,26.8702684537753,2.73675429797997));
#63267=CARTESIAN_POINT('Ctrl Pts',(-22.6657646993551,28.1173557828319,2.55360623026512));
#63268=CARTESIAN_POINT('Ctrl Pts',(-19.2297687690452,25.2748309986811,2.3547193188902));
#63269=CARTESIAN_POINT('Ctrl Pts',(-19.7639310999953,20.8475648235122,2.1558324075154));
#63270=CARTESIAN_POINT('Ctrl Pts',(-23.7774017995599,18.9038395020308,1.95694549614038));
#63271=CARTESIAN_POINT('Ctrl Pts',(-26.9764049458243,20.8594715760247,1.78972253431358));
#63272=CARTESIAN_POINT('Ctrl Pts',(-27.4760272010612,22.863454934077,1.68879520961172));
#63273=CARTESIAN_POINT('Ctrl Pts',(-27.4767827643537,23.550738941023,1.65416352203481));
#63274=CARTESIAN_POINT('',(-27.4832594378696,23.5537205931952,0.404163526210238));
#63275=CARTESIAN_POINT('Ctrl Pts',(-27.4767827643537,23.550738941023,1.65416352203481));
#63276=CARTESIAN_POINT('Ctrl Pts',(-27.477473580183,24.1791266299795,1.62249957248676));
#63277=CARTESIAN_POINT('Ctrl Pts',(-27.0381896343703,26.1222740522175,1.52453998581368));
#63278=CARTESIAN_POINT('Ctrl Pts',(-23.9850432680626,28.1818513752549,1.3602847620158));
#63279=CARTESIAN_POINT('Ctrl Pts',(-19.8886335395912,26.4196247955838,1.16139785064084));
#63280=CARTESIAN_POINT('Ctrl Pts',(-19.1569412107686,22.0206883880481,0.962510939266074));
#63281=CARTESIAN_POINT('Ctrl Pts',(-22.4623294945035,19.027291742867,0.763624027891007));
#63282=CARTESIAN_POINT('Ctrl Pts',(-26.4909783005602,20.1154429344271,0.577508486344934));
#63283=CARTESIAN_POINT('Ctrl Pts',(-27.4751100911716,22.4969944765995,0.457688581923687));
#63284=CARTESIAN_POINT('Ctrl Pts',(-27.4848522193952,23.5537064323839,0.404164314627433));
#63285=CARTESIAN_POINT('',(-27.4850143494599,23.5481581335268,-0.845837085113357));
#63286=CARTESIAN_POINT('Ctrl Pts',(-27.483251002585,23.5537206681901,0.404163522034823));
#63287=CARTESIAN_POINT('Ctrl Pts',(-27.4831014233451,23.7233492057095,0.395567971166493));
#63288=CARTESIAN_POINT('Ctrl Pts',(-27.471974586661,23.8925128226098,0.386972420298163));
#63289=CARTESIAN_POINT('Ctrl Pts',(-27.450069179886,24.0600751581893,0.378376869429831));
#63290=CARTESIAN_POINT('Ctrl Pts',(-27.439427950837,24.1414737467288,0.374201314666986));
#63291=CARTESIAN_POINT('Ctrl Pts',(-27.4262438101914,24.2224950106797,0.370025759904141));
#63292=CARTESIAN_POINT('Ctrl Pts',(-27.4105431465028,24.3030110382688,0.365850205141295));
#63293=CARTESIAN_POINT('Ctrl Pts',(-27.3884624973385,24.4162448602627,0.359977908172612));
#63294=CARTESIAN_POINT('Ctrl Pts',(-27.3613584050731,24.5286960190449,0.354105611203929));
#63295=CARTESIAN_POINT('Ctrl Pts',(-27.3292989305641,24.6398842654413,0.348233314235246));
#63296=CARTESIAN_POINT('Ctrl Pts',(-27.2972810025879,24.7509284207005,0.342368627297074));
#63297=CARTESIAN_POINT('Ctrl Pts',(-27.260320576457,24.8607125247166,0.336503940358903));
#63298=CARTESIAN_POINT('Ctrl Pts',(-27.2185369188538,24.9687653638256,0.33063925342073));
#63299=CARTESIAN_POINT('Ctrl Pts',(-27.1767962331267,25.0767070773538,0.324780597945935));
#63300=CARTESIAN_POINT('Ctrl Pts',(-27.1302423305995,25.1829206842347,0.318921942471139));
#63301=CARTESIAN_POINT('Ctrl Pts',(-27.0790444026469,25.2869496646158,0.313063286996343));
#63302=CARTESIAN_POINT('Ctrl Pts',(-27.0258466385337,25.3950421085986,0.306975787278432));
#63303=CARTESIAN_POINT('Ctrl Pts',(-26.9676347794541,25.5007753430996,0.300888287560521));
#63304=CARTESIAN_POINT('Ctrl Pts',(-26.9046540947007,25.6036592508074,0.294800787842609));
#63305=CARTESIAN_POINT('Ctrl Pts',(-26.8441112114125,25.702560817867,0.28894891775923));
#63306=CARTESIAN_POINT('Ctrl Pts',(-26.7791620489905,25.7988291497208,0.283097047675851));
#63307=CARTESIAN_POINT('Ctrl Pts',(-26.710071134818,25.8920542729509,0.277245177592472));
#63308=CARTESIAN_POINT('Ctrl Pts',(-26.6409907403654,25.9852652018083,0.271394198509522));
#63309=CARTESIAN_POINT('Ctrl Pts',(-26.5677700941059,26.075433511317,0.265543219426572));
#63310=CARTESIAN_POINT('Ctrl Pts',(-26.4907160495626,26.1621796555024,0.259692240343622));
#63311=CARTESIAN_POINT('Ctrl Pts',(-26.4136550771192,26.248933599001,0.253840735201346));
#63312=CARTESIAN_POINT('Ctrl Pts',(-26.3327602957871,26.3322644564463,0.247989230059069));
#63313=CARTESIAN_POINT('Ctrl Pts',(-26.2483772161981,26.4118276550958,0.242137724916793));
#63314=CARTESIAN_POINT('Ctrl Pts',(-26.1639661148251,26.4914172749517,0.236284276617029));
#63315=CARTESIAN_POINT('Ctrl Pts',(-26.0760647124238,26.5672364647243,0.230430828317265));
#63316=CARTESIAN_POINT('Ctrl Pts',(-25.9850530095633,26.6389797182499,0.224577380017501));
#63317=CARTESIAN_POINT('Ctrl Pts',(-25.8939378066339,26.7108045594335,0.218717275075979));
#63318=CARTESIAN_POINT('Ctrl Pts',(-25.7997055681635,26.7785439565373,0.212857170134457));
#63319=CARTESIAN_POINT('Ctrl Pts',(-25.7027668751975,26.8419346246388,0.206997065192935));
#63320=CARTESIAN_POINT('Ctrl Pts',(-25.6057629000891,26.9053679823878,0.20113301383751));
#63321=CARTESIAN_POINT('Ctrl Pts',(-25.5060491960494,26.9644465695172,0.195268962482086));
#63322=CARTESIAN_POINT('Ctrl Pts',(-25.4040611007033,27.0189529784708,0.189404911126661));
#63323=CARTESIAN_POINT('Ctrl Pts',(-25.3019226952632,27.0735397189908,0.183532217330108));
#63324=CARTESIAN_POINT('Ctrl Pts',(-25.1975035800155,27.1235406547688,0.177659523533554));
#63325=CARTESIAN_POINT('Ctrl Pts',(-25.0912592804576,27.1687863784705,0.171786829737001));
#63326=CARTESIAN_POINT('Ctrl Pts',(-25.062171368485,27.1811739007531,0.17017898441347));
#63327=CARTESIAN_POINT('Ctrl Pts',(-25.0329467319798,27.1932052741425,0.168571139089938));
#63328=CARTESIAN_POINT('Ctrl Pts',(-25.0035948967839,27.2048776793442,0.166963293766407));
#63329=CARTESIAN_POINT('Ctrl Pts',(-24.8963938555364,27.247508539838,0.161090996797697));
#63330=CARTESIAN_POINT('Ctrl Pts',(-24.7871358980256,27.2854900307209,0.155218699828987));
#63331=CARTESIAN_POINT('Ctrl Pts',(-24.6762618557182,27.3186198176963,0.149346402860276));
#63332=CARTESIAN_POINT('Ctrl Pts',(-24.5655314973643,27.3517066710989,0.143481715922072));
#63333=CARTESIAN_POINT('Ctrl Pts',(-24.4531896114827,27.3799542067631,0.137617028983867));
#63334=CARTESIAN_POINT('Ctrl Pts',(-24.3396971067328,27.4032080547884,0.131752342045662));
#63335=CARTESIAN_POINT('Ctrl Pts',(-24.2263213219194,27.4264379876867,0.125893686570838));
#63336=CARTESIAN_POINT('Ctrl Pts',(-24.1117976744959,27.4446843656312,0.120035031096014));
#63337=CARTESIAN_POINT('Ctrl Pts',(-23.9966016973842,27.4578427638306,0.114176375621191));
#63338=CARTESIAN_POINT('Ctrl Pts',(-23.8769060639434,27.4715151406535,0.108088875903287));
#63339=CARTESIAN_POINT('Ctrl Pts',(-23.756484942131,27.4796938225144,0.102001376185383));
#63340=CARTESIAN_POINT('Ctrl Pts',(-23.6358832543151,27.4823202294003,0.0959138764674789));
#63341=CARTESIAN_POINT('Ctrl Pts',(-23.5199497115402,27.484844975617,0.0900620063840775));
#63342=CARTESIAN_POINT('Ctrl Pts',(-23.4038497730578,27.4822392700093,0.0842101363006761));
#63343=CARTESIAN_POINT('Ctrl Pts',(-23.2880713446477,27.4745040558907,0.0783582662172749));
#63344=CARTESIAN_POINT('Ctrl Pts',(-23.1723105445562,27.4667700195288,0.0725072871343076));
#63345=CARTESIAN_POINT('Ctrl Pts',(-23.0568715695533,27.4539080551118,0.0666563080513403));
#63346=CARTESIAN_POINT('Ctrl Pts',(-22.9422396053731,27.4359711629678,0.0608053289683731));
#63347=CARTESIAN_POINT('Ctrl Pts',(-22.8275973346761,27.4180326581245,0.0549538238260758));
#63348=CARTESIAN_POINT('Ctrl Pts',(-22.7137626274781,27.3950183824119,0.0491023186837784));
#63349=CARTESIAN_POINT('Ctrl Pts',(-22.6012121417523,27.3670327635466,0.0432508135414812));
#63350=CARTESIAN_POINT('Ctrl Pts',(-22.4886242804604,27.3390378512664,0.0373973652417081));
#63351=CARTESIAN_POINT('Ctrl Pts',(-22.3773218895887,27.3060684128702,0.0315439169419352));
#63352=CARTESIAN_POINT('Ctrl Pts',(-22.2677674030154,27.2682790101795,0.0256904686421622));
#63353=CARTESIAN_POINT('Ctrl Pts',(-22.1580883292015,27.2304466327321,0.0198303637006198));
#63354=CARTESIAN_POINT('Ctrl Pts',(-22.0501615181881,27.1877834852662,0.0139702587590774));
#63355=CARTESIAN_POINT('Ctrl Pts',(-21.9444304124587,27.1404926798422,0.00811015381753506));
#63356=CARTESIAN_POINT('Ctrl Pts',(-21.838628103447,27.0931700270206,0.00224610246208278));
#63357=CARTESIAN_POINT('Ctrl Pts',(-21.7350248126622,27.0412136956528,-0.0036179488933695));
#63358=CARTESIAN_POINT('Ctrl Pts',(-21.6340387671704,26.9848724245862,-0.00948200024882183));
#63359=CARTESIAN_POINT('Ctrl Pts',(-21.5329038884063,26.9284481177328,-0.0153546940453922));
#63360=CARTESIAN_POINT('Ctrl Pts',(-21.4343943037761,26.8676261895828,-0.0212273878419625));
#63361=CARTESIAN_POINT('Ctrl Pts',(-21.3388987693554,26.8026983095343,-0.0271000816385329));
#63362=CARTESIAN_POINT('Ctrl Pts',(-21.3127536894765,26.784922142088,-0.028707926961845));
#63363=CARTESIAN_POINT('Ctrl Pts',(-21.2868343382308,26.7668384324236,-0.0303157722851571));
#63364=CARTESIAN_POINT('Ctrl Pts',(-21.2611482366596,26.7484536708432,-0.0319236176084692));
#63365=CARTESIAN_POINT('Ctrl Pts',(-21.167335471086,26.6813074235435,-0.0377959145771856));
#63366=CARTESIAN_POINT('Ctrl Pts',(-21.076322447735,26.6099174767044,-0.043668211545902));
#63367=CARTESIAN_POINT('Ctrl Pts',(-20.9885176819414,26.5345453389706,-0.0495405085146185));
#63368=CARTESIAN_POINT('Ctrl Pts',(-20.9008267041509,26.4592708775414,-0.0554051954528298));
#63369=CARTESIAN_POINT('Ctrl Pts',(-20.8163360266228,26.3800247545737,-0.0612698823910413));
#63370=CARTESIAN_POINT('Ctrl Pts',(-20.7354246640142,26.2971112967806,-0.0671345693292529));
#63371=CARTESIAN_POINT('Ctrl Pts',(-20.6545965136769,26.2142831102883,-0.0729932248040839));
#63372=CARTESIAN_POINT('Ctrl Pts',(-20.5773406433354,26.1277953850026,-0.078851880278915));
#63373=CARTESIAN_POINT('Ctrl Pts',(-20.5040019530224,26.0379917487227,-0.0847105357537462));
#63374=CARTESIAN_POINT('Ctrl Pts',(-20.42779858887,25.944680303312,-0.0907980354716464));
#63375=CARTESIAN_POINT('Ctrl Pts',(-20.3558250052433,25.8477889173408,-0.0968855351895468));
#63376=CARTESIAN_POINT('Ctrl Pts',(-20.2884250401308,25.7477443781594,-0.102973034907447));
#63377=CARTESIAN_POINT('Ctrl Pts',(-20.2236339341362,25.6515722758229,-0.108824904990857));
#63378=CARTESIAN_POINT('Ctrl Pts',(-20.1630692194076,25.5524869552794,-0.114676775074266));
#63379=CARTESIAN_POINT('Ctrl Pts',(-20.1069938360773,25.4508994097487,-0.120528645157676));
#63380=CARTESIAN_POINT('Ctrl Pts',(-20.0509269907339,25.3493273318455,-0.126379624240656));
#63381=CARTESIAN_POINT('Ctrl Pts',(-19.9993483174046,25.2452541482869,-0.132230603323635));
#63382=CARTESIAN_POINT('Ctrl Pts',(-19.9524754894816,25.1391167028958,-0.138081582406615));
#63383=CARTESIAN_POINT('Ctrl Pts',(-19.9055984472403,25.0329697147269,-0.143933087548922));
#63384=CARTESIAN_POINT('Ctrl Pts',(-19.8634282585003,24.9247584739471,-0.149784592691228));
#63385=CARTESIAN_POINT('Ctrl Pts',(-19.8261347203128,24.8149404485148,-0.155636097833535));
#63386=CARTESIAN_POINT('Ctrl Pts',(-19.7888287977531,24.7050859549068,-0.161489546133317));
#63387=CARTESIAN_POINT('Ctrl Pts',(-19.7564028787359,24.5936240068804,-0.1673429944331));
#63388=CARTESIAN_POINT('Ctrl Pts',(-19.7289768929224,24.481027205033,-0.173196442732883));
#63389=CARTESIAN_POINT('Ctrl Pts',(-19.7015197178075,24.3683023561719,-0.179056547674435));
#63390=CARTESIAN_POINT('Ctrl Pts',(-19.6790739228884,24.2544404794189,-0.184916652615988));
#63391=CARTESIAN_POINT('Ctrl Pts',(-19.661708326042,24.1399244410548,-0.19077675755754));
#63392=CARTESIAN_POINT('Ctrl Pts',(-19.6443310345531,24.0253312833061,-0.196640808912999));
#63393=CARTESIAN_POINT('Ctrl Pts',(-19.6320407971446,23.9100834967976,-0.202504860268458));
#63394=CARTESIAN_POINT('Ctrl Pts',(-19.6248544151101,23.7946673968688,-0.208368911623917));
#63395=CARTESIAN_POINT('Ctrl Pts',(-19.6176574417831,23.679081196648,-0.214241605420499));
#63396=CARTESIAN_POINT('Ctrl Pts',(-19.6155793438109,23.5633265996907,-0.22011429921708));
#63397=CARTESIAN_POINT('Ctrl Pts',(-19.6185848739744,23.4478883326802,-0.225986993013661));
#63398=CARTESIAN_POINT('Ctrl Pts',(-19.6194077378567,23.4162832662209,-0.227594838336907));
#63399=CARTESIAN_POINT('Ctrl Pts',(-19.6206113580627,23.3847018694414,-0.229202683660152));
#63400=CARTESIAN_POINT('Ctrl Pts',(-19.6221943396339,23.3531539782036,-0.230810528983397));
#63401=CARTESIAN_POINT('Ctrl Pts',(-19.6279758272855,23.2379323313163,-0.236682825952087));
#63402=CARTESIAN_POINT('Ctrl Pts',(-19.6388409899222,23.1227722550315,-0.242555122920777));
#63403=CARTESIAN_POINT('Ctrl Pts',(-19.6547906357902,23.0081587966629,-0.248427419889468));
#63404=CARTESIAN_POINT('Ctrl Pts',(-19.6707196121839,22.8936938682339,-0.254292106827657));
#63405=CARTESIAN_POINT('Ctrl Pts',(-19.6917199120295,22.7797745546788,-0.260156793765846));
#63406=CARTESIAN_POINT('Ctrl Pts',(-19.7177403736471,22.6668842288776,-0.266021480704035));
#63407=CARTESIAN_POINT('Ctrl Pts',(-19.7437340748488,22.5541100037094,-0.27188013617884));
#63408=CARTESIAN_POINT('Ctrl Pts',(-19.7747375762156,22.4423630617817,-0.277738791653646));
#63409=CARTESIAN_POINT('Ctrl Pts',(-19.8106482110032,22.3321193186715,-0.283597447128451));
#63410=CARTESIAN_POINT('Ctrl Pts',(-19.8479615468154,22.2175693578536,-0.289684946846359));
#63411=CARTESIAN_POINT('Ctrl Pts',(-19.8905731223735,22.1046428727228,-0.295772446564268));
#63412=CARTESIAN_POINT('Ctrl Pts',(-19.9383097333281,21.9938598366036,-0.301859946282177));
#63413=CARTESIAN_POINT('Ctrl Pts',(-19.9841985971429,21.8873648937118,-0.307711816365564));
#63414=CARTESIAN_POINT('Ctrl Pts',(-20.0348229439625,21.7828509667625,-0.313563686448951));
#63415=CARTESIAN_POINT('Ctrl Pts',(-20.0899791285838,21.6807614309593,-0.319415556532339));
#63416=CARTESIAN_POINT('Ctrl Pts',(-20.1451269151745,21.5786874392163,-0.325266535615292));
#63417=CARTESIAN_POINT('Ctrl Pts',(-20.2048049711578,21.4790374682561,-0.331117514698246));
#63418=CARTESIAN_POINT('Ctrl Pts',(-20.2687634341927,21.3822307829614,-0.336968493781199));
#63419=CARTESIAN_POINT('Ctrl Pts',(-20.3327276477089,21.2854153938139,-0.342819998923483));
#63420=CARTESIAN_POINT('Ctrl Pts',(-20.4009728054362,21.1914441434438,-0.348671504065767));
#63421=CARTESIAN_POINT('Ctrl Pts',(-20.4732058144103,21.1007071657839,-0.35452300920805));
#63422=CARTESIAN_POINT('Ctrl Pts',(-20.5454628103944,21.009940056349,-0.360376457507813));
#63423=CARTESIAN_POINT('Ctrl Pts',(-20.6217100335435,20.9224096785141,-0.366229905807576));
#63424=CARTESIAN_POINT('Ctrl Pts',(-20.701614704112,20.8384723917736,-0.372083354107339));
#63425=CARTESIAN_POINT('Ctrl Pts',(-20.7816102436418,20.7544396501115,-0.377943459048868));
#63426=CARTESIAN_POINT('Ctrl Pts',(-20.8652712472577,20.6740084549124,-0.383803563990396));
#63427=CARTESIAN_POINT('Ctrl Pts',(-20.9522286704359,20.5974977135062,-0.389663668931924));
#63428=CARTESIAN_POINT('Ctrl Pts',(-21.0392446539961,20.5209354469042,-0.395527720287355));
#63429=CARTESIAN_POINT('Ctrl Pts',(-21.1295611561015,20.4482991496557,-0.401391771642785));
#63430=CARTESIAN_POINT('Ctrl Pts',(-21.2227781133087,20.379865831028,-0.407255822998215));
#63431=CARTESIAN_POINT('Ctrl Pts',(-21.3161324537031,20.3113316553492,-0.413128516794771));
#63432=CARTESIAN_POINT('Ctrl Pts',(-21.4123954382311,20.2470130498172,-0.419001210591326));
#63433=CARTESIAN_POINT('Ctrl Pts',(-21.5111402055849,20.1871423756765,-0.424873904387882));
#63434=CARTESIAN_POINT('Ctrl Pts',(-21.5381748710902,20.1707507866097,-0.426481749711327));
#63435=CARTESIAN_POINT('Ctrl Pts',(-21.565395437831,20.1546923286918,-0.428089595034772));
#63436=CARTESIAN_POINT('Ctrl Pts',(-21.5927928766977,20.1389711450213,-0.429697440358217));
#63437=CARTESIAN_POINT('Ctrl Pts',(-21.6928559206118,20.0815530228508,-0.435569737326925));
#63438=CARTESIAN_POINT('Ctrl Pts',(-21.7956151059868,20.0284451632611,-0.441442034295634));
#63439=CARTESIAN_POINT('Ctrl Pts',(-21.9006627912706,19.9799104348792,-0.447314331264342));
#63440=CARTESIAN_POINT('Ctrl Pts',(-22.005574343097,19.9314386036507,-0.453179018202544));
#63441=CARTESIAN_POINT('Ctrl Pts',(-22.11276812529,19.8875282899,-0.459043705140747));
#63442=CARTESIAN_POINT('Ctrl Pts',(-22.2218098130786,19.8483977339803,-0.464908392078949));
#63443=CARTESIAN_POINT('Ctrl Pts',(-22.3307393583174,19.8093074213879,-0.470767047553771));
#63444=CARTESIAN_POINT('Ctrl Pts',(-22.4415126422997,19.774987227871,-0.476625703028593));
#63445=CARTESIAN_POINT('Ctrl Pts',(-22.553673773538,19.7456080307202,-0.482484358503414));
#63446=CARTESIAN_POINT('Ctrl Pts',(-22.6702160173526,19.7150812562518,-0.488571858221319));
#63447=CARTESIAN_POINT('Ctrl Pts',(-22.7882563270237,19.6898895372098,-0.494659357939225));
#63448=CARTESIAN_POINT('Ctrl Pts',(-22.9072636159754,19.6701682214939,-0.50074685765713));
#63449=CARTESIAN_POINT('Ctrl Pts',(-23.0216644744878,19.6512102612818,-0.506598727740525));
#63450=CARTESIAN_POINT('Ctrl Pts',(-23.1369584003652,19.6373071654731,-0.51245059782392));
#63451=CARTESIAN_POINT('Ctrl Pts',(-23.2526622957446,19.6285272670349,-0.518302467907315));
#63452=CARTESIAN_POINT('Ctrl Pts',(-23.3683485741538,19.619748705416,-0.524153446990283));
#63453=CARTESIAN_POINT('Ctrl Pts',(-23.4844442858662,19.6160918214419,-0.530004426073252));
#63454=CARTESIAN_POINT('Ctrl Pts',(-23.6004616351134,19.6175730321756,-0.53585540515622));
#63455=CARTESIAN_POINT('Ctrl Pts',(-23.7164894154368,19.6190543760844,-0.541706910298511));
#63456=CARTESIAN_POINT('Ctrl Pts',(-23.8324384059155,19.6256747277654,-0.547558415440801));
#63457=CARTESIAN_POINT('Ctrl Pts',(-23.9478219511535,19.6373983871201,-0.553409920583092));
#63458=CARTESIAN_POINT('Ctrl Pts',(-24.0632438127547,19.6491259396468,-0.559263368882843));
#63459=CARTESIAN_POINT('Ctrl Pts',(-24.1780994446946,19.6659601278811,-0.565116817182595));
#63460=CARTESIAN_POINT('Ctrl Pts',(-24.2919091541914,19.6878136060533,-0.570970265482346));
#63461=CARTESIAN_POINT('Ctrl Pts',(-24.4058482900415,19.7096919363756,-0.576830370423882));
#63462=CARTESIAN_POINT('Ctrl Pts',(-24.5187387231532,19.7366008716773,-0.582690475365417));
#63463=CARTESIAN_POINT('Ctrl Pts',(-24.6301126672292,19.7684023115397,-0.588550580306953));
#63464=CARTESIAN_POINT('Ctrl Pts',(-24.7415616146861,19.8002251676816,-0.594414631662402));
#63465=CARTESIAN_POINT('Ctrl Pts',(-24.8514916484476,19.8369469583216,-0.600278683017851));
#63466=CARTESIAN_POINT('Ctrl Pts',(-24.9594534647184,19.8783808386249,-0.6061427343733));
#63467=CARTESIAN_POINT('Ctrl Pts',(-25.0675743951551,19.9198757841968,-0.612015428169868));
#63468=CARTESIAN_POINT('Ctrl Pts',(-25.1737209411578,19.9660965152552,-0.617888121966435));
#63469=CARTESIAN_POINT('Ctrl Pts',(-25.27746687668,20.0168095073233,-0.623760815763002));
#63470=CARTESIAN_POINT('Ctrl Pts',(-25.3058707783694,20.0306938762273,-0.625368661086382));
#63471=CARTESIAN_POINT('Ctrl Pts',(-25.3340948987324,20.0449147184682,-0.626976506409762));
#63472=CARTESIAN_POINT('Ctrl Pts',(-25.3621308714945,20.059466677225,-0.628584351733142));
#63473=CARTESIAN_POINT('Ctrl Pts',(-25.4645260182614,20.1126144657925,-0.634456648701863));
#63474=CARTESIAN_POINT('Ctrl Pts',(-25.5647522475575,20.1703604430574,-0.640328945670583));
#63475=CARTESIAN_POINT('Ctrl Pts',(-25.6623680560565,20.2325037449793,-0.646201242639304));
#63476=CARTESIAN_POINT('Ctrl Pts',(-25.75985736222,20.2945665141172,-0.652065929577516));
#63477=CARTESIAN_POINT('Ctrl Pts',(-25.854742629459,20.3610150555275,-0.657930616515728));
#63478=CARTESIAN_POINT('Ctrl Pts',(-25.9466054775514,20.431601932656,-0.66379530345394));
#63479=CARTESIAN_POINT('Ctrl Pts',(-26.0383738504552,20.5021162156001,-0.669653958928763));
#63480=CARTESIAN_POINT('Ctrl Pts',(-26.1271256610989,20.5767601184639,-0.675512614403587));
#63481=CARTESIAN_POINT('Ctrl Pts',(-26.2124707188754,20.6552424585093,-0.681371269878411));
#63482=CARTESIAN_POINT('Ctrl Pts',(-26.3011494297795,20.7367903878832,-0.687458769596311));
#63483=CARTESIAN_POINT('Ctrl Pts',(-26.3861494371434,20.8224824888239,-0.693546269314211));
#63484=CARTESIAN_POINT('Ctrl Pts',(-26.4670697956996,20.9119451105623,-0.699633769032112));
#63485=CARTESIAN_POINT('Ctrl Pts',(-26.54485795953,20.9979448910952,-0.705485639115518));
#63486=CARTESIAN_POINT('Ctrl Pts',(-26.6188761218968,21.0874283926874,-0.711337509198923));
#63487=CARTESIAN_POINT('Ctrl Pts',(-26.688805658253,21.1800261138666,-0.717189379282329));
#63488=CARTESIAN_POINT('Ctrl Pts',(-26.7587245472015,21.2726097362008,-0.723040358365308));
#63489=CARTESIAN_POINT('Ctrl Pts',(-26.8245557988721,21.3683063055329,-0.728891337448287));
#63490=CARTESIAN_POINT('Ctrl Pts',(-26.8860219270224,21.4667143052171,-0.734742316531267));
#63491=CARTESIAN_POINT('Ctrl Pts',(-26.9474935815692,21.5651311527275,-0.740593821673573));
#63492=CARTESIAN_POINT('Ctrl Pts',(-27.0045991134024,21.6662595645785,-0.746445326815878));
#63493=CARTESIAN_POINT('Ctrl Pts',(-27.0571054997417,21.7696708120035,-0.752296831958184));
#63494=CARTESIAN_POINT('Ctrl Pts',(-27.1096293223089,21.8731164000528,-0.758150280257977));
#63495=CARTESIAN_POINT('Ctrl Pts',(-27.1575507754387,21.9788459626734,-0.76400372855777));
#63496=CARTESIAN_POINT('Ctrl Pts',(-27.2006840503086,22.086408712188,-0.769857176857563));
#63497=CARTESIAN_POINT('Ctrl Pts',(-27.2438663770781,22.1940937839054,-0.77571728179911));
#63498=CARTESIAN_POINT('Ctrl Pts',(-27.2822495031859,22.3036158196673,-0.781577386740657));
#63499=CARTESIAN_POINT('Ctrl Pts',(-27.3156967565068,22.4145066138827,-0.787437491682205));
#63500=CARTESIAN_POINT('Ctrl Pts',(-27.3491665344594,22.5254720861076,-0.793301543037662));
#63501=CARTESIAN_POINT('Ctrl Pts',(-27.3776937193796,22.6378077525327,-0.799165594393119));
#63502=CARTESIAN_POINT('Ctrl Pts',(-27.4011926392129,22.7510346087824,-0.805029645748576));
#63503=CARTESIAN_POINT('Ctrl Pts',(-27.4247261917633,22.8644283388157,-0.810902339545148));
#63504=CARTESIAN_POINT('Ctrl Pts',(-27.4432166232067,22.9787154734938,-0.816775033341719));
#63505=CARTESIAN_POINT('Ctrl Pts',(-27.4566300083566,23.0934111918128,-0.822647727138291));
#63506=CARTESIAN_POINT('Ctrl Pts',(-27.4603023688319,23.1248129608619,-0.824255572461539));
#63507=CARTESIAN_POINT('Ctrl Pts',(-27.4635944692151,23.1562453549675,-0.825863417784788));
#63508=CARTESIAN_POINT('Ctrl Pts',(-27.4665062939636,23.1876984398535,-0.827471263108036));
#63509=CARTESIAN_POINT('Ctrl Pts',(-27.477592826223,23.3074534630305,-0.833593001393755));
#63510=CARTESIAN_POINT('Ctrl Pts',(-27.4831875036166,23.4277246956559,-0.839714739679475));
#63511=CARTESIAN_POINT('Ctrl Pts',(-27.4832519681591,23.548147118064,-0.845836477965195));
#63512=CARTESIAN_POINT('',(-27.48156856957,23.5477950957604,-2.09583596348537));
#63513=CARTESIAN_POINT('Ctrl Pts',(-27.488361223027,23.5481790525876,-0.845838238126122));
#63514=CARTESIAN_POINT('Ctrl Pts',(-27.4806823124676,24.7334074016489,-0.906011550245059));
#63515=CARTESIAN_POINT('Ctrl Pts',(-26.2794691055314,27.2379105123852,-1.03248049948896));
#63516=CARTESIAN_POINT('Ctrl Pts',(-22.0150358044262,27.9415917844077,-1.22524508585781));
#63517=CARTESIAN_POINT('Ctrl Pts',(-19.0258954158673,24.6323539689758,-1.42413199723265));
#63518=CARTESIAN_POINT('Ctrl Pts',(-20.1942556145273,20.3287566797515,-1.62301890860764));
#63519=CARTESIAN_POINT('Ctrl Pts',(-24.4464924384507,18.9854409406596,-1.8219058199825));
#63520=CARTESIAN_POINT('Ctrl Pts',(-27.1634961703733,21.244963443143,-1.97951117201133));
#63521=CARTESIAN_POINT('Ctrl Pts',(-27.4811027227655,23.0518391628667,-2.07082088691515));
#63522=CARTESIAN_POINT('Ctrl Pts',(-27.478300869659,23.5477773275668,-2.09583496469404));
#63523=CARTESIAN_POINT('',(-27.482122854251,23.5532788466855,-3.34583691089324));
#63524=CARTESIAN_POINT('Ctrl Pts',(-27.4832517696687,23.5478042481997,-2.09583647796519));
#63525=CARTESIAN_POINT('Ctrl Pts',(-27.4833246542727,23.6648883574814,-2.10173454261193));
#63526=CARTESIAN_POINT('Ctrl Pts',(-27.4781648693244,23.7819916671266,-2.10763260725867));
#63527=CARTESIAN_POINT('Ctrl Pts',(-27.4677938782179,23.898618428816,-2.11353067190542));
#63528=CARTESIAN_POINT('Ctrl Pts',(-27.4574217011788,24.015258526885,-2.11942941100139));
#63529=CARTESIAN_POINT('Ctrl Pts',(-27.4418371675545,24.1314215660302,-2.12532815009736));
#63530=CARTESIAN_POINT('Ctrl Pts',(-27.4211136371411,24.2466168776645,-2.13122688919334));
#63531=CARTESIAN_POINT('Ctrl Pts',(-27.4003830219145,24.3618515714521,-2.13712764490825));
#63532=CARTESIAN_POINT('Ctrl Pts',(-27.3745099852318,24.4761174818321,-2.14302840062316));
#63533=CARTESIAN_POINT('Ctrl Pts',(-27.3436189016895,24.5889346693036,-2.14892915633808));
#63534=CARTESIAN_POINT('Ctrl Pts',(-27.3126878313712,24.7018978923003,-2.1548375502505));
#63535=CARTESIAN_POINT('Ctrl Pts',(-27.2767258456684,24.8134082559318,-2.16074594416292));
#63536=CARTESIAN_POINT('Ctrl Pts',(-27.2359072188032,24.9230010619762,-2.16665433807534));
#63537=CARTESIAN_POINT('Ctrl Pts',(-27.1950620589579,25.0326651056876,-2.17256657257013));
#63538=CARTESIAN_POINT('Ctrl Pts',(-27.1493541253973,25.1404087364141,-2.17847880706492));
#63539=CARTESIAN_POINT('Ctrl Pts',(-27.0990051098812,25.2457890658955,-2.18439104155971));
#63540=CARTESIAN_POINT('Ctrl Pts',(-27.0485626404997,25.3513649940202,-2.19031424987715));
#63541=CARTESIAN_POINT('Ctrl Pts',(-26.9934620634722,25.4545684973145,-2.19623745819458));
#63542=CARTESIAN_POINT('Ctrl Pts',(-26.9339705319384,25.554982312693,-2.20216066651202));
#63543=CARTESIAN_POINT('Ctrl Pts',(-26.8753181558165,25.6539797450261,-2.2080003252521));
#63544=CARTESIAN_POINT('Ctrl Pts',(-26.8123981750014,25.7502654222508,-2.21383998399218));
#63545=CARTESIAN_POINT('Ctrl Pts',(-26.7455051231394,25.8434707674631,-2.21967964273225));
#63546=CARTESIAN_POINT('Ctrl Pts',(-26.6782382017041,25.93719704335,-2.22555193970097));
#63547=CARTESIAN_POINT('Ctrl Pts',(-26.6067311872943,26.0281181180212,-2.23142423666969));
#63548=CARTESIAN_POINT('Ctrl Pts',(-26.5312461140655,26.1158258130217,-2.23729653363841));
#63549=CARTESIAN_POINT('Ctrl Pts',(-26.4558588634967,26.203419845815,-2.24316122057662));
#63550=CARTESIAN_POINT('Ctrl Pts',(-26.376504073216,26.2878084697762,-2.24902590751484));
#63551=CARTESIAN_POINT('Ctrl Pts',(-26.2934865574468,26.3686130622071,-2.25489059445305));
#63552=CARTESIAN_POINT('Ctrl Pts',(-26.2105544199956,26.4493345521732,-2.26074924992788));
#63553=CARTESIAN_POINT('Ctrl Pts',(-26.1239673440281,26.5264790555594,-2.26660790540271));
#63554=CARTESIAN_POINT('Ctrl Pts',(-26.0340694009186,26.5997021148413,-2.27246656087754));
#63555=CARTESIAN_POINT('Ctrl Pts',(-25.9406599649704,26.6757853313126,-2.27855406059544));
#63556=CARTESIAN_POINT('Ctrl Pts',(-25.843676034825,26.7476341636557,-2.28464156031334));
#63557=CARTESIAN_POINT('Ctrl Pts',(-25.7435448399721,26.8149053234086,-2.29072906003125));
#63558=CARTESIAN_POINT('Ctrl Pts',(-25.6472894361563,26.8795726097293,-2.29658093011465));
#63559=CARTESIAN_POINT('Ctrl Pts',(-25.5481262555831,26.9400097591984,-2.30243280019806));
#63560=CARTESIAN_POINT('Ctrl Pts',(-25.4464666295152,26.9959543608177,-2.30828467028146));
#63561=CARTESIAN_POINT('Ctrl Pts',(-25.3448224820499,27.0518904443626,-2.31413564936444));
#63562=CARTESIAN_POINT('Ctrl Pts',(-25.2406830069288,27.1033351408816,-2.31998662844741));
#63563=CARTESIAN_POINT('Ctrl Pts',(-25.1344853277419,27.1500713393465,-2.32583760753039));
#63564=CARTESIAN_POINT('Ctrl Pts',(-25.0282781003617,27.1968117398453,-2.33168911267268));
#63565=CARTESIAN_POINT('Ctrl Pts',(-24.9200126794348,27.2388426342079,-2.33754061781498));
#63566=CARTESIAN_POINT('Ctrl Pts',(-24.810146751056,27.2759948142493,-2.34339212295727));
#63567=CARTESIAN_POINT('Ctrl Pts',(-24.700244338594,27.3131593317209,-2.34924557125705));
#63568=CARTESIAN_POINT('Ctrl Pts',(-24.58874075323,27.3454417810223,-2.35509901955682));
#63569=CARTESIAN_POINT('Ctrl Pts',(-24.4761087495102,27.3727228407916,-2.3609524678566));
#63570=CARTESIAN_POINT('Ctrl Pts',(-24.3633486587444,27.4000349250499,-2.36681257279815));
#63571=CARTESIAN_POINT('Ctrl Pts',(-24.2494579902851,27.4223341699959,-2.3726726777397));
#63572=CARTESIAN_POINT('Ctrl Pts',(-24.1349196985764,27.4395523792207,-2.37853278268125));
#63573=CARTESIAN_POINT('Ctrl Pts',(-24.0203042724967,27.4567821838319,-2.38439683403673));
#63574=CARTESIAN_POINT('Ctrl Pts',(-23.9050407648425,27.4689240961187,-2.3902608853922));
#63575=CARTESIAN_POINT('Ctrl Pts',(-23.7896155121726,27.4759619406516,-2.39612493674767));
#63576=CARTESIAN_POINT('Ctrl Pts',(-23.6740201457215,27.4830101575624,-2.40199763054426));
#63577=CARTESIAN_POINT('Ctrl Pts',(-23.558262970268,27.4849392866438,-2.40787032434085));
#63578=CARTESIAN_POINT('Ctrl Pts',(-23.4428286667338,27.4817851988912,-2.41374301813744));
#63579=CARTESIAN_POINT('Ctrl Pts',(-23.411224685408,27.480921662426,-2.41535086346068));
#63580=CARTESIAN_POINT('Ctrl Pts',(-23.3796448637463,27.4796774004135,-2.41695870878393));
#63581=CARTESIAN_POINT('Ctrl Pts',(-23.348099035807,27.478053820469,-2.41856655410717));
#63582=CARTESIAN_POINT('Ctrl Pts',(-23.2328849246582,27.4721240563002,-2.42443885107587));
#63583=CARTESIAN_POINT('Ctrl Pts',(-23.1177389263555,27.4611107005926,-2.43031114804456));
#63584=CARTESIAN_POINT('Ctrl Pts',(-23.0031460888512,27.4450135693189,-2.43618344501325));
#63585=CARTESIAN_POINT('Ctrl Pts',(-22.8887017545635,27.428937298649,-2.44204813195144));
#63586=CARTESIAN_POINT('Ctrl Pts',(-22.774809561097,27.4077904108904,-2.44791281888963));
#63587=CARTESIAN_POINT('Ctrl Pts',(-22.6619528150904,27.3816246897443,-2.45377750582782));
#63588=CARTESIAN_POINT('Ctrl Pts',(-22.5492121351819,27.3554858784044,-2.45963616130264));
#63589=CARTESIAN_POINT('Ctrl Pts',(-22.4375051848865,27.3243385930816,-2.46549481677746));
#63590=CARTESIAN_POINT('Ctrl Pts',(-22.3273077472633,27.2882861129015,-2.47135347225228));
#63591=CARTESIAN_POINT('Ctrl Pts',(-22.2128059006658,27.2508253910909,-2.47744097197019));
#63592=CARTESIAN_POINT('Ctrl Pts',(-22.0999343468339,27.2080685232089,-2.48352847168809));
#63593=CARTESIAN_POINT('Ctrl Pts',(-21.9892128357608,27.1601893826267,-2.489615971406));
#63594=CARTESIAN_POINT('Ctrl Pts',(-21.8827770364571,27.1141635060968,-2.49546784148939));
#63595=CARTESIAN_POINT('Ctrl Pts',(-21.7783283456541,27.0634046998971,-2.50131971157278));
#63596=CARTESIAN_POINT('Ctrl Pts',(-21.6763098761126,27.0081171796514,-2.50717158165617));
#63597=CARTESIAN_POINT('Ctrl Pts',(-21.5743069398106,26.9528380774332,-2.51302256073914));
#63598=CARTESIAN_POINT('Ctrl Pts',(-21.4747338523888,26.8930318291002,-2.51887353982211));
#63599=CARTESIAN_POINT('Ctrl Pts',(-21.3780095568292,26.8289488363479,-2.52472451890508));
#63600=CARTESIAN_POINT('Ctrl Pts',(-21.2812765648244,26.7648600819177,-2.53057602404739));
#63601=CARTESIAN_POINT('Ctrl Pts',(-21.1873932184841,26.6964940470069,-2.53642752918969));
#63602=CARTESIAN_POINT('Ctrl Pts',(-21.0967492742306,26.6241443264091,-2.542279034332));
#63603=CARTESIAN_POINT('Ctrl Pts',(-21.0060752290967,26.5517705800443,-2.54813248263177));
#63604=CARTESIAN_POINT('Ctrl Pts',(-20.9186430479949,26.4754107752407,-2.55398593093153));
#63605=CARTESIAN_POINT('Ctrl Pts',(-20.8348086618625,26.3953981500754,-2.5598393792313));
#63606=CARTESIAN_POINT('Ctrl Pts',(-20.7508789378289,26.3152945331809,-2.56569948417284));
#63607=CARTESIAN_POINT('Ctrl Pts',(-20.6705554744434,26.231530090146,-2.57155958911437));
#63608=CARTESIAN_POINT('Ctrl Pts',(-20.59415670384,26.1444742755979,-2.5774196940559));
#63609=CARTESIAN_POINT('Ctrl Pts',(-20.5177064834463,26.0573598344074,-2.58328374541133));
#63610=CARTESIAN_POINT('Ctrl Pts',(-20.4451864766657,25.9669499298223,-2.58914779676677));
#63611=CARTESIAN_POINT('Ctrl Pts',(-20.3768731776859,25.8736449814439,-2.5950118481222));
#63612=CARTESIAN_POINT('Ctrl Pts',(-20.30845919854,25.780202520197,-2.60088454191876));
#63613=CARTESIAN_POINT('Ctrl Pts',(-20.244264529249,25.6838568423362,-2.60675723571532));
#63614=CARTESIAN_POINT('Ctrl Pts',(-20.1845209815277,25.5850351078467,-2.61262992951188));
#63615=CARTESIAN_POINT('Ctrl Pts',(-20.1681641975486,25.5579793700284,-2.61423777483526));
#63616=CARTESIAN_POINT('Ctrl Pts',(-20.1521407836831,25.5307381598423,-2.61584562015864));
#63617=CARTESIAN_POINT('Ctrl Pts',(-20.1364548714063,25.5033205117227,-2.61745346548201));
#63618=CARTESIAN_POINT('Ctrl Pts',(-20.0791655701436,25.4031836580085,-2.62332576245072));
#63619=CARTESIAN_POINT('Ctrl Pts',(-20.0261899976171,25.300356212039,-2.62919805941943));
#63620=CARTESIAN_POINT('Ctrl Pts',(-19.9777904976329,25.1952461533203,-2.63507035638813));
#63621=CARTESIAN_POINT('Ctrl Pts',(-19.9294537195569,25.0902723088901,-2.64093504332632));
#63622=CARTESIAN_POINT('Ctrl Pts',(-19.8856813922345,24.9830221063017,-2.64679973026451));
#63623=CARTESIAN_POINT('Ctrl Pts',(-19.8466911968959,24.8739301508248,-2.6526644172027));
#63624=CARTESIAN_POINT('Ctrl Pts',(-19.8077411005326,24.764950389595,-2.65852307267751));
#63625=CARTESIAN_POINT('Ctrl Pts',(-19.7735634920431,24.654133029921,-2.66438172815231));
#63626=CARTESIAN_POINT('Ctrl Pts',(-19.7443286618798,24.5419341828186,-2.67024038362711));
#63627=CARTESIAN_POINT('Ctrl Pts',(-19.7139518935004,24.4253527499244,-2.67632788334502));
#63628=CARTESIAN_POINT('Ctrl Pts',(-19.6889121040238,24.3072801182162,-2.68241538306293));
#63629=CARTESIAN_POINT('Ctrl Pts',(-19.6693439577706,24.1882475480119,-2.68850288278084));
#63630=CARTESIAN_POINT('Ctrl Pts',(-19.6505332382712,24.0738223868119,-2.69435475286423));
#63631=CARTESIAN_POINT('Ctrl Pts',(-19.6367785282974,23.9585106642039,-2.70020662294762));
#63632=CARTESIAN_POINT('Ctrl Pts',(-19.6281475390507,23.8427955655904,-2.706058493031));
#63633=CARTESIAN_POINT('Ctrl Pts',(-19.6195178639506,23.7270980856528,-2.71190947211396));
#63634=CARTESIAN_POINT('Ctrl Pts',(-19.6160103891629,23.6109977639522,-2.71776045119692));
#63635=CARTESIAN_POINT('Ctrl Pts',(-19.6176409039817,23.4949824169804,-2.72361143027989));
#63636=CARTESIAN_POINT('Ctrl Pts',(-19.6192715653995,23.3789566391125,-2.72946293542216));
#63637=CARTESIAN_POINT('Ctrl Pts',(-19.6260411289376,23.2630162645278,-2.73531444056444));
#63638=CARTESIAN_POINT('Ctrl Pts',(-19.6379132682393,23.1476479022758,-2.74116594570672));
#63639=CARTESIAN_POINT('Ctrl Pts',(-19.64978935002,23.032241228702,-2.74701939400649));
#63640=CARTESIAN_POINT('Ctrl Pts',(-19.6667713345861,22.9174073561639,-2.75287284230626));
#63641=CARTESIAN_POINT('Ctrl Pts',(-19.6887712589127,22.8036258646389,-2.75872629060602));
#63642=CARTESIAN_POINT('Ctrl Pts',(-19.7107962019305,22.6897149788509,-2.76458639554755));
#63643=CARTESIAN_POINT('Ctrl Pts',(-19.737850396163,22.5768592689307,-2.77044650048908));
#63644=CARTESIAN_POINT('Ctrl Pts',(-19.7697951393013,22.4655263430634,-2.77630660543061));
#63645=CARTESIAN_POINT('Ctrl Pts',(-19.8017613952247,22.3541184414384,-2.78217065678605));
#63646=CARTESIAN_POINT('Ctrl Pts',(-19.8386246268657,22.2442357567988,-2.7880347081415));
#63647=CARTESIAN_POINT('Ctrl Pts',(-19.8801974113251,22.1363273521134,-2.79389875949694));
#63648=CARTESIAN_POINT('Ctrl Pts',(-19.92183146577,22.0282599119802,-2.7997714532935));
#63649=CARTESIAN_POINT('Ctrl Pts',(-19.9681887609088,21.9221729363647,-2.80564414709005));
#63650=CARTESIAN_POINT('Ctrl Pts',(-20.0190352239381,21.8184923504325,-2.81151684088661));
#63651=CARTESIAN_POINT('Ctrl Pts',(-20.032956134959,21.7901063403666,-2.81312468621005));
#63652=CARTESIAN_POINT('Ctrl Pts',(-20.0472132876738,21.7619005444932,-2.81473253153349));
#63653=CARTESIAN_POINT('Ctrl Pts',(-20.0618013144989,21.7338833221862,-2.81634037685693));
#63654=CARTESIAN_POINT('Ctrl Pts',(-20.1150808336513,21.6315566572847,-2.82221267382564));
#63655=CARTESIAN_POINT('Ctrl Pts',(-20.1729557464653,21.5314048255695,-2.82808497079435));
#63656=CARTESIAN_POINT('Ctrl Pts',(-20.2352246208861,21.4338690715047,-2.83395726776306));
#63657=CARTESIAN_POINT('Ctrl Pts',(-20.297412799791,21.3364597160312,-2.83982195470126));
#63658=CARTESIAN_POINT('Ctrl Pts',(-20.3639833961407,21.2416600414739,-2.84568664163947));
#63659=CARTESIAN_POINT('Ctrl Pts',(-20.4346884351633,21.1498881092768,-2.85155132857767));
#63660=CARTESIAN_POINT('Ctrl Pts',(-20.5053207584793,21.058210558767,-2.85740998405249));
#63661=CARTESIAN_POINT('Ctrl Pts',(-20.5800788162142,20.9695548825192,-2.86326863952731));
#63662=CARTESIAN_POINT('Ctrl Pts',(-20.6586709237259,20.8843108960878,-2.86912729500212));
#63663=CARTESIAN_POINT('Ctrl Pts',(-20.7403329081801,20.7957372044645,-2.87521479472003));
#63664=CARTESIAN_POINT('Ctrl Pts',(-20.8261343265639,20.7108475465617,-2.88130229443793));
#63665=CARTESIAN_POINT('Ctrl Pts',(-20.9157010124322,20.6300423864557,-2.88738979415583));
#63666=CARTESIAN_POINT('Ctrl Pts',(-21.0018008290713,20.5523649620742,-2.89324166423924));
#63667=CARTESIAN_POINT('Ctrl Pts',(-21.091379512186,20.4784620193127,-2.89909353432265));
#63668=CARTESIAN_POINT('Ctrl Pts',(-21.1840671505649,20.4086517069346,-2.90494540440606));
#63669=CARTESIAN_POINT('Ctrl Pts',(-21.2767406764081,20.3388520238114,-2.91079638348904));
#63670=CARTESIAN_POINT('Ctrl Pts',(-21.3725218861999,20.2731439807019,-2.91664736257202));
#63671=CARTESIAN_POINT('Ctrl Pts',(-21.4710089065238,20.2118045468982,-2.922498341655));
#63672=CARTESIAN_POINT('Ctrl Pts',(-21.5695047817786,20.1504595980891,-2.92834984679731));
#63673=CARTESIAN_POINT('Ctrl Pts',(-21.6707066002681,20.0934842579507,-2.93420135193961));
#63674=CARTESIAN_POINT('Ctrl Pts',(-21.7741853336982,20.0411109973296,-2.94005285708192));
#63675=CARTESIAN_POINT('Ctrl Pts',(-21.877698430163,19.9887203446889,-2.94590630538169));
#63676=CARTESIAN_POINT('Ctrl Pts',(-21.9834895764158,19.9409349969722,-2.95175975368146));
#63677=CARTESIAN_POINT('Ctrl Pts',(-22.0911077460315,19.8979401827195,-2.95761320198123));
#63678=CARTESIAN_POINT('Ctrl Pts',(-22.1988483008749,19.8548964740267,-2.96347330692278));
#63679=CARTESIAN_POINT('Ctrl Pts',(-22.3084196420435,19.8166543260515,-2.96933341186432));
#63680=CARTESIAN_POINT('Ctrl Pts',(-22.4193533884474,19.7833498082616,-2.97519351680587));
#63681=CARTESIAN_POINT('Ctrl Pts',(-22.5303618417868,19.7500228619634,-2.98105756816135));
#63682=CARTESIAN_POINT('Ctrl Pts',(-22.6427341274588,19.7216402679381,-2.98692161951682));
#63683=CARTESIAN_POINT('Ctrl Pts',(-22.7559911312308,19.6982870817279,-2.9927856708723));
#63684=CARTESIAN_POINT('Ctrl Pts',(-22.8694150532178,19.6748994775831,-2.99865836466887));
#63685=CARTESIAN_POINT('Ctrl Pts',(-22.9837258890047,19.6565561401114,-3.00453105846545));
#63686=CARTESIAN_POINT('Ctrl Pts',(-23.0984387743304,19.6432903705443,-3.01040375226203));
#63687=CARTESIAN_POINT('Ctrl Pts',(-23.1298452434189,19.6396584247463,-3.0120115975853));
#63688=CARTESIAN_POINT('Ctrl Pts',(-23.1612818481735,19.6364067781375,-3.01361944290856));
#63689=CARTESIAN_POINT('Ctrl Pts',(-23.1927386543061,19.633535433476,-3.01522728823182));
#63690=CARTESIAN_POINT('Ctrl Pts',(-23.3076276331307,19.6230484865613,-3.02109958520052));
#63691=CARTESIAN_POINT('Ctrl Pts',(-23.4231708933924,19.6176033109717,-3.02697188216923));
#63692=CARTESIAN_POINT('Ctrl Pts',(-23.5388883261552,19.6172689498784,-3.03284417913793));
#63693=CARTESIAN_POINT('Ctrl Pts',(-23.6544557983154,19.6169350220905,-3.03870886607613));
#63694=CARTESIAN_POINT('Ctrl Pts',(-23.7701965845477,19.6216987387958,-3.04457355301433));
#63695=CARTESIAN_POINT('Ctrl Pts',(-23.8856249218682,19.6315774545911,-3.05043823995253));
#63696=CARTESIAN_POINT('Ctrl Pts',(-24.0009345483693,19.6414460107456,-3.05629689542733));
#63697=CARTESIAN_POINT('Ctrl Pts',(-24.1159319557078,19.6564190676342,-3.06215555090212));
#63698=CARTESIAN_POINT('Ctrl Pts',(-24.2301315176028,19.6764619379063,-3.06801420637692));
#63699=CARTESIAN_POINT('Ctrl Pts',(-24.3487918149717,19.6972877003448,-3.07410170609483));
#63700=CARTESIAN_POINT('Ctrl Pts',(-24.4665902124818,19.7235874144039,-3.08018920581274));
#63701=CARTESIAN_POINT('Ctrl Pts',(-24.5829875401612,19.7552627553856,-3.08627670553064));
#63702=CARTESIAN_POINT('Ctrl Pts',(-24.6948794615081,19.7857120348701,-3.09212857561405));
#63703=CARTESIAN_POINT('Ctrl Pts',(-24.8054763229485,19.821128410417,-3.09798044569746));
#63704=CARTESIAN_POINT('Ctrl Pts',(-24.9143105078985,19.8613726424116,-3.10383231578086));
#63705=CARTESIAN_POINT('Ctrl Pts',(-25.0231281218543,19.9016107468561,-3.10968329486384));
#63706=CARTESIAN_POINT('Ctrl Pts',(-25.1301832053341,19.9466751028323,-3.11553427394681));
#63707=CARTESIAN_POINT('Ctrl Pts',(-25.2350255098076,19.9963773211362,-3.12138525302979));
#63708=CARTESIAN_POINT('Ctrl Pts',(-25.3398772406127,20.0460840081476,-3.12723675817206));
#63709=CARTESIAN_POINT('Ctrl Pts',(-25.4425154233602,20.1004292093306,-3.13308826331434));
#63710=CARTESIAN_POINT('Ctrl Pts',(-25.5425125684457,20.1591776363309,-3.13893976845661));
#63711=CARTESIAN_POINT('Ctrl Pts',(-25.6425429204071,20.2179455724055,-3.14479321675641));
#63712=CARTESIAN_POINT('Ctrl Pts',(-25.7399301345507,20.2811194325328,-3.15064666505621));
#63713=CARTESIAN_POINT('Ctrl Pts',(-25.834274576095,20.3484198844918,-3.15650011335601));
#63714=CARTESIAN_POINT('Ctrl Pts',(-25.9287263077554,20.4157968716784,-3.16236021829756));
#63715=CARTESIAN_POINT('Ctrl Pts',(-26.0201280234437,20.4873095772382,-3.1682203232391));
#63716=CARTESIAN_POINT('Ctrl Pts',(-26.1081120657983,20.5626374956173,-3.17408042818064));
#63717=CARTESIAN_POINT('Ctrl Pts',(-26.1961553598988,20.6380161426349,-3.17994447953609));
#63718=CARTESIAN_POINT('Ctrl Pts',(-26.2807760966672,20.7172148366861,-3.18580853089154));
#63719=CARTESIAN_POINT('Ctrl Pts',(-26.361643735895,20.7998764670546,-3.19167258224699));
#63720=CARTESIAN_POINT('Ctrl Pts',(-26.4426305578804,20.8826599241655,-3.19754527604357));
#63721=CARTESIAN_POINT('Ctrl Pts',(-26.5198529681875,20.9689161967156,-3.20341796984014));
#63722=CARTESIAN_POINT('Ctrl Pts',(-26.5930208602435,21.0582553609942,-3.20929066363671));
#63723=CARTESIAN_POINT('Ctrl Pts',(-26.6130530051392,21.082714929712,-3.21089850896005));
#63724=CARTESIAN_POINT('Ctrl Pts',(-26.6327814875512,21.1074054199052,-3.21250635428339));
#63725=CARTESIAN_POINT('Ctrl Pts',(-26.6522009352553,21.1323184751813,-3.21411419960673));
#63726=CARTESIAN_POINT('Ctrl Pts',(-26.7231378177672,21.2233228385422,-3.21998746317924));
#63727=CARTESIAN_POINT('Ctrl Pts',(-26.7901893465413,21.3176091291791,-3.22586072675175));
#63728=CARTESIAN_POINT('Ctrl Pts',(-26.8530365008391,21.4148118153175,-3.23173399032427));
#63729=CARTESIAN_POINT('Ctrl Pts',(-26.9158037361498,21.5118908945829,-3.23759978521692));
#63730=CARTESIAN_POINT('Ctrl Pts',(-26.9743770037245,21.6118786541688,-3.24346558010956));
#63731=CARTESIAN_POINT('Ctrl Pts',(-27.0284774515868,21.714376608153,-3.24933137500221));
#63732=CARTESIAN_POINT('Ctrl Pts',(-27.0825221532819,21.8167689462264,-3.25519112566426));
#63733=CARTESIAN_POINT('Ctrl Pts',(-27.1321030083236,21.9216659732544,-3.26105087632632));
#63734=CARTESIAN_POINT('Ctrl Pts',(-27.1769848197709,22.0286409154721,-3.26691062698837));
#63735=CARTESIAN_POINT('Ctrl Pts',(-27.2218312081501,22.1355314274822,-3.27276575282937));
#63736=CARTESIAN_POINT('Ctrl Pts',(-27.261985770649,22.2444962138211,-3.27862087867038));
#63737=CARTESIAN_POINT('Ctrl Pts',(-27.297259893632,22.3550852506896,-3.28447600451138));
#63738=CARTESIAN_POINT('Ctrl Pts',(-27.3325166140797,22.4656197283104,-3.2903282417183));
#63739=CARTESIAN_POINT('Ctrl Pts',(-27.3628975582545,22.5777764705715,-3.29618047892522));
#63740=CARTESIAN_POINT('Ctrl Pts',(-27.3882630050007,22.6910874679318,-3.30203271613214));
#63741=CARTESIAN_POINT('Ctrl Pts',(-27.4136210567992,22.8043654310269,-3.30788324719967));
#63742=CARTESIAN_POINT('Ctrl Pts',(-27.4339664328418,22.9187965768231,-3.3137337782672));
#63743=CARTESIAN_POINT('Ctrl Pts',(-27.4492100355465,23.0339005362938,-3.31958430933472));
#63744=CARTESIAN_POINT('Ctrl Pts',(-27.464456042393,23.149022649363,-3.32543576311762));
#63745=CARTESIAN_POINT('Ctrl Pts',(-27.4745986124711,23.2648173792551,-3.33128721690051));
#63746=CARTESIAN_POINT('Ctrl Pts',(-27.4796003104943,23.3807974248407,-3.3371386706834));
#63747=CARTESIAN_POINT('Ctrl Pts',(-27.4820785439443,23.4382630349532,-3.34003793977733));
#63748=CARTESIAN_POINT('Ctrl Pts',(-27.4832955026874,23.4957740748039,-3.34293720887125));
#63749=CARTESIAN_POINT('Ctrl Pts',(-27.4832513732947,23.5532711355702,-3.34583647796518));
#63750=CARTESIAN_POINT('',(-27.4892650790848,23.551517445815,-4.59583647796518));
#63751=CARTESIAN_POINT('Ctrl Pts',(-27.4794097119894,23.5532973854538,-3.34583795172231));
#63752=CARTESIAN_POINT('Ctrl Pts',(-27.4825587700888,23.9968499807919,-3.36822567147541));
#63753=CARTESIAN_POINT('Ctrl Pts',(-27.2081891243134,25.7500858833574,-3.45690902835341));
#63754=CARTESIAN_POINT('Ctrl Pts',(-24.6265305769216,28.0759984814206,-3.61188802235648));
#63755=CARTESIAN_POINT('Ctrl Pts',(-20.3244404402133,26.9021008550186,-3.81077493373142));
#63756=CARTESIAN_POINT('Ctrl Pts',(-18.9865981118165,22.6481388093524,-4.0096618451063));
#63757=CARTESIAN_POINT('Ctrl Pts',(-21.8423672611993,19.2231427878892,-4.20854875648117));
#63758=CARTESIAN_POINT('Ctrl Pts',(-26.189767356571,19.7647057021154,-4.40394030076747));
#63759=CARTESIAN_POINT('Ctrl Pts',(-27.4840831004861,22.3152979151724,-4.5330362079288));
#63760=CARTESIAN_POINT('Ctrl Pts',(-27.4892650790848,23.551517445815,-4.59583647796518));
#63761=CARTESIAN_POINT('',(-27.4832669639411,23.5466206728664,-5.84583647796516));
#63762=CARTESIAN_POINT('Ctrl Pts',(-27.4892650790848,23.551517445815,-4.59583647796518));
#63763=CARTESIAN_POINT('Ctrl Pts',(-27.489553500097,23.6203235362853,-4.59933184505377));
#63764=CARTESIAN_POINT('Ctrl Pts',(-27.4879074477743,23.6891155407879,-4.60282721214237));
#63765=CARTESIAN_POINT('Ctrl Pts',(-27.4155519149962,25.0605826362573,-4.67261821635592));
#63766=CARTESIAN_POINT('Ctrl Pts',(-25.855147816285,27.5910703399071,-4.80520949060578));
#63767=CARTESIAN_POINT('Ctrl Pts',(-21.3965383245707,27.6736329344889,-5.0040964019808));
#63768=CARTESIAN_POINT('Ctrl Pts',(-18.9170095843528,23.967158543905,-5.20298331335561));
#63769=CARTESIAN_POINT('Ctrl Pts',(-20.6950382785201,19.8775828759019,-5.40187022473053));
#63770=CARTESIAN_POINT('Ctrl Pts',(-25.0967667891071,19.1628792305347,-5.6007571361054));
#63771=CARTESIAN_POINT('Ctrl Pts',(-27.3145959907761,21.6309496960074,-5.74874588718358));
#63772=CARTESIAN_POINT('Ctrl Pts',(-27.4860826067821,23.2423189068336,-5.83043900113687));
#63773=CARTESIAN_POINT('Ctrl Pts',(-27.4832669639411,23.5466206728664,-5.84583647796516));
#63774=CARTESIAN_POINT('',(-27.476760765631,23.5506274849305,-7.09583647796518));
#63775=CARTESIAN_POINT('Ctrl Pts',(-27.4832669639411,23.5466206728664,-5.84583647796516));
#63776=CARTESIAN_POINT('Ctrl Pts',(-27.473959527258,24.5525257467186,-5.89673463826183));
#63777=CARTESIAN_POINT('Ctrl Pts',(-26.5684793902742,26.8835250199973,-6.01392843568338));
#63778=CARTESIAN_POINT('Ctrl Pts',(-22.6422664878202,28.1127422222305,-6.19741787023015));
#63779=CARTESIAN_POINT('Ctrl Pts',(-19.2209484554937,25.2525677339697,-6.39630478160496));
#63780=CARTESIAN_POINT('Ctrl Pts',(-19.7778938047406,20.8281099073478,-6.59519169297986));
#63781=CARTESIAN_POINT('Ctrl Pts',(-23.8013169807825,18.9050703528649,-6.79407860435475));
#63782=CARTESIAN_POINT('Ctrl Pts',(-26.9837010307554,20.873118155621,-6.96096019934984));
#63783=CARTESIAN_POINT('Ctrl Pts',(-27.4761842519322,22.8701085782786,-7.06154615722));
#63784=CARTESIAN_POINT('Ctrl Pts',(-27.476760765631,23.5506274849305,-7.09583647796518));
#63785=CARTESIAN_POINT('',(-27.4832509725328,23.5537545826837,-8.34583647796518));
#63786=CARTESIAN_POINT('Ctrl Pts',(-27.476760765631,23.5506274849305,-7.09583647796518));
#63787=CARTESIAN_POINT('Ctrl Pts',(-27.4772988621821,24.1857986480022,-7.12784179434496));
#63788=CARTESIAN_POINT('Ctrl Pts',(-27.031270723818,26.1359470768735,-7.22614274784961));
#63789=CARTESIAN_POINT('Ctrl Pts',(-23.961195575086,28.1840281679555,-7.39073933847951));
#63790=CARTESIAN_POINT('Ctrl Pts',(-19.8739114783422,26.4007379800943,-7.5896262498543));
#63791=CARTESIAN_POINT('Ctrl Pts',(-19.1648731073088,21.9980933464675,-7.7885131612292));
#63792=CARTESIAN_POINT('Ctrl Pts',(-22.485626608426,19.0217514026655,-7.98740007260408));
#63793=CARTESIAN_POINT('Ctrl Pts',(-26.5012424661459,20.1285926572705,-8.173174280116));
#63794=CARTESIAN_POINT('Ctrl Pts',(-27.4749296595235,22.5036284115385,-8.29265285050309));
#63795=CARTESIAN_POINT('Ctrl Pts',(-27.4846475833386,23.5537421191806,-8.34583578376515));
#63796=CARTESIAN_POINT('',(-27.4850836380432,23.5482599068045,-9.59583708370669));
#63797=CARTESIAN_POINT('Ctrl Pts',(-27.4832509725328,23.5537545826837,-8.34583647796518));
#63798=CARTESIAN_POINT('Ctrl Pts',(-27.4831019658486,23.7210973936125,-8.35431462942859));
#63799=CARTESIAN_POINT('Ctrl Pts',(-27.4722693976411,23.8879836340533,-8.36279278089199));
#63800=CARTESIAN_POINT('Ctrl Pts',(-27.4509467894136,24.0533164518824,-8.3712709323554));
#63801=CARTESIAN_POINT('Ctrl Pts',(-27.4392914407801,24.1436905567658,-8.3759052533549));
#63802=CARTESIAN_POINT('Ctrl Pts',(-27.424502514206,24.2336011584677,-8.3805395743544));
#63803=CARTESIAN_POINT('Ctrl Pts',(-27.4066170495043,24.32287255847,-8.3851738953539));
#63804=CARTESIAN_POINT('Ctrl Pts',(-27.3839538027933,24.4359912163431,-8.3910461923225));
#63805=CARTESIAN_POINT('Ctrl Pts',(-27.3562712084288,24.5483013623581,-8.3969184892911));
#63806=CARTESIAN_POINT('Ctrl Pts',(-27.3236397985297,24.6593231040583,-8.40279078625971));
#63807=CARTESIAN_POINT('Ctrl Pts',(-27.2910506763462,24.7702009703983,-8.40865547319781));
#63808=CARTESIAN_POINT('Ctrl Pts',(-27.2535256078182,24.8797933598515,-8.41452016013591));
#63809=CARTESIAN_POINT('Ctrl Pts',(-27.2111862836991,24.9876296789424,-8.42038484707402));
#63810=CARTESIAN_POINT('Ctrl Pts',(-27.1688905029244,25.0953550951297,-8.42624350254875));
#63811=CARTESIAN_POINT('Ctrl Pts',(-27.1217904648406,25.2013276507248,-8.43210215802348));
#63812=CARTESIAN_POINT('Ctrl Pts',(-27.0700577085932,25.3050917028648,-8.43796081349821));
#63813=CARTESIAN_POINT('Ctrl Pts',(-27.0163042253202,25.4129088702777,-8.44404831321615));
#63814=CARTESIAN_POINT('Ctrl Pts',(-26.9575488579407,25.5183410485715,-8.45013581293408));
#63815=CARTESIAN_POINT('Ctrl Pts',(-26.8940393954591,25.6208993894933,-8.45622331265201));
#63816=CARTESIAN_POINT('Ctrl Pts',(-26.8329882019111,25.7194879915208,-8.46207518273532));
#63817=CARTESIAN_POINT('Ctrl Pts',(-26.7675443426298,25.8154207111699,-8.46792705281863));
#63818=CARTESIAN_POINT('Ctrl Pts',(-26.6979744519005,25.9082889421537,-8.47377892290194));
#63819=CARTESIAN_POINT('Ctrl Pts',(-26.6284151538198,26.0011430331048,-8.47962990198482));
#63820=CARTESIAN_POINT('Ctrl Pts',(-26.5547313211814,26.0909332323791,-8.4854808810677));
#63821=CARTESIAN_POINT('Ctrl Pts',(-26.4772317572196,26.1772815786106,-8.49133186015058));
#63822=CARTESIAN_POINT('Ctrl Pts',(-26.3997252253012,26.2636376883895,-8.49718336529279));
#63823=CARTESIAN_POINT('Ctrl Pts',(-26.3184025561994,26.3465510222942,-8.503034870435));
#63824=CARTESIAN_POINT('Ctrl Pts',(-26.2336110297142,26.4256787907215,-8.50888637557721));
#63825=CARTESIAN_POINT('Ctrl Pts',(-26.148791345809,26.5048328357581,-8.51473982387689));
#63826=CARTESIAN_POINT('Ctrl Pts',(-26.0605008160413,26.5801985337569,-8.52059327217658));
#63827=CARTESIAN_POINT('Ctrl Pts',(-25.9691210085896,26.6514723387188,-8.52644672047627));
#63828=CARTESIAN_POINT('Ctrl Pts',(-25.8776372824541,26.7228271974737,-8.53230682541771));
#63829=CARTESIAN_POINT('Ctrl Pts',(-25.7830575925853,26.7900806208148,-8.53816693035916));
#63830=CARTESIAN_POINT('Ctrl Pts',(-25.6857938698919,26.8529714408429,-8.54402703530061));
#63831=CARTESIAN_POINT('Ctrl Pts',(-25.5884646461688,26.9159046139021,-8.54989108665597));
#63832=CARTESIAN_POINT('Ctrl Pts',(-25.4884481463292,26.9744691252552,-8.55575513801134));
#63833=CARTESIAN_POINT('Ctrl Pts',(-25.3861808213717,27.0284498112001,-8.56161918936669));
#63834=CARTESIAN_POINT('Ctrl Pts',(-25.2837627747917,27.0825100539004,-8.56749188316317));
#63835=CARTESIAN_POINT('Ctrl Pts',(-25.1790876548214,27.1319728122813,-8.57336457695964));
#63836=CARTESIAN_POINT('Ctrl Pts',(-25.0726118529757,27.1766710261467,-8.57923727075612));
#63837=CARTESIAN_POINT('Ctrl Pts',(-25.0434605595363,27.1889086494003,-8.58084511608034));
#63838=CARTESIAN_POINT('Ctrl Pts',(-25.0141743767119,27.2007894246667,-8.58245296140456));
#63839=CARTESIAN_POINT('Ctrl Pts',(-24.9847628447309,27.2123105817244,-8.58406080672879));
#63840=CARTESIAN_POINT('Ctrl Pts',(-24.8773437743168,27.2543890420385,-8.58993310369751));
#63841=CARTESIAN_POINT('Ctrl Pts',(-24.7678917483023,27.291807606021,-8.59580540066624));
#63842=CARTESIAN_POINT('Ctrl Pts',(-24.6568486338633,27.3243662113101,-8.60167769763497));
#63843=CARTESIAN_POINT('Ctrl Pts',(-24.5459494224818,27.3568826232325,-8.60754238457319));
#63844=CARTESIAN_POINT('Ctrl Pts',(-24.4334636161244,27.3845514859259,-8.61340707151141));
#63845=CARTESIAN_POINT('Ctrl Pts',(-24.3198529119889,27.4072208041396,-8.61927175844964));
#63846=CARTESIAN_POINT('Ctrl Pts',(-24.2063590493505,27.4298668083786,-8.62513041392447));
#63847=CARTESIAN_POINT('Ctrl Pts',(-24.0917429929958,27.4475234148771,-8.63098906939931));
#63848=CARTESIAN_POINT('Ctrl Pts',(-23.9764808070906,27.460088648113,-8.63684772487415));
#63849=CARTESIAN_POINT('Ctrl Pts',(-23.8567163786826,27.4731446904263,-8.64293522459205));
#63850=CARTESIAN_POINT('Ctrl Pts',(-23.7362547512321,27.4807033759924,-8.64902272430995));
#63851=CARTESIAN_POINT('Ctrl Pts',(-23.6156411414375,27.4827089306535,-8.65511022402785));
#63852=CARTESIAN_POINT('Ctrl Pts',(-23.4996961381493,27.4846368560524,-8.66096209411126));
#63853=CARTESIAN_POINT('Ctrl Pts',(-23.3836111512199,27.4814335410521,-8.66681396419467));
#63854=CARTESIAN_POINT('Ctrl Pts',(-23.2678740751089,27.4731024405304,-8.67266583427808));
#63855=CARTESIAN_POINT('Ctrl Pts',(-23.1521546210202,27.4647726084946,-8.67851681336106));
#63856=CARTESIAN_POINT('Ctrl Pts',(-23.0367833846264,27.4513165729938,-8.68436779244404));
#63857=CARTESIAN_POINT('Ctrl Pts',(-22.922245272405,27.4327898312291,-8.69021877152701));
#63858=CARTESIAN_POINT('Ctrl Pts',(-22.807696862105,27.414261423732,-8.69607027666932));
#63859=CARTESIAN_POINT('Ctrl Pts',(-22.6939821329867,27.3906614696848,-8.70192178181162));
#63860=CARTESIAN_POINT('Ctrl Pts',(-22.5815771991487,27.3620968490972,-8.70777328695393));
#63861=CARTESIAN_POINT('Ctrl Pts',(-22.4691349380791,27.3335227428211,-8.71362673525371));
#63862=CARTESIAN_POINT('Ctrl Pts',(-22.3580037376061,27.2999807935126,-8.7194801835535));
#63863=CARTESIAN_POINT('Ctrl Pts',(-22.2486452298479,27.2616279414016,-8.72533363185328));
#63864=CARTESIAN_POINT('Ctrl Pts',(-22.1391623577198,27.2232314737696,-8.73119373679483));
#63865=CARTESIAN_POINT('Ctrl Pts',(-22.0314565923752,27.1800133201904,-8.73705384173637));
#63866=CARTESIAN_POINT('Ctrl Pts',(-21.9259703248689,27.1321788727279,-8.74291394667792));
#63867=CARTESIAN_POINT('Ctrl Pts',(-21.8204130189636,27.0843122117588,-8.74877799803338));
#63868=CARTESIAN_POINT('Ctrl Pts',(-21.7170785547875,27.0318232534521,-8.75464204938883));
#63869=CARTESIAN_POINT('Ctrl Pts',(-21.6163838734407,26.9749628862533,-8.76050610074429));
#63870=CARTESIAN_POINT('Ctrl Pts',(-21.5155407882341,26.9180187182238,-8.76637879454087));
#63871=CARTESIAN_POINT('Ctrl Pts',(-21.4173455998717,26.8566905013052,-8.77225148833744));
#63872=CARTESIAN_POINT('Ctrl Pts',(-21.322185557861,26.7912719022185,-8.77812418213402));
#63873=CARTESIAN_POINT('Ctrl Pts',(-21.2961323301937,26.7733613841095,-8.77973202745723));
#63874=CARTESIAN_POINT('Ctrl Pts',(-21.2703064112939,26.7551444898331,-8.78133987278043));
#63875=CARTESIAN_POINT('Ctrl Pts',(-21.2447152886934,26.7366277483215,-8.78294771810364));
#63876=CARTESIAN_POINT('Ctrl Pts',(-21.1512494126519,26.6689994737106,-8.78882001507236));
#63877=CARTESIAN_POINT('Ctrl Pts',(-21.0606050868939,26.5971419679294,-8.79469231204108));
#63878=CARTESIAN_POINT('Ctrl Pts',(-20.9731894751818,26.5213188390591,-8.8005646090098));
#63879=CARTESIAN_POINT('Ctrl Pts',(-20.8858871471601,26.445593970942,-8.80642929594803));
#63880=CARTESIAN_POINT('Ctrl Pts',(-20.8018055217932,26.3659139679909,-8.81229398288625));
#63881=CARTESIAN_POINT('Ctrl Pts',(-20.7213220421437,26.2825851039283,-8.81815866982447));
#63882=CARTESIAN_POINT('Ctrl Pts',(-20.6409213347147,26.199341938386,-8.82401732529931));
#63883=CARTESIAN_POINT('Ctrl Pts',(-20.5641116980415,26.1124576714474,-8.82987598077414));
#63884=CARTESIAN_POINT('Ctrl Pts',(-20.4912362587049,26.0222777017899,-8.83573463624898));
#63885=CARTESIAN_POINT('Ctrl Pts',(-20.4155142405203,25.9285752230884,-8.84182213596687));
#63886=CARTESIAN_POINT('Ctrl Pts',(-20.3440403751643,25.8313146247633,-8.84790963568477));
#63887=CARTESIAN_POINT('Ctrl Pts',(-20.2771562991104,25.7309244584741,-8.85399713540267));
#63888=CARTESIAN_POINT('Ctrl Pts',(-20.2128611135902,25.6344201072624,-8.85984900548609));
#63889=CARTESIAN_POINT('Ctrl Pts',(-20.1528072596188,25.5350243325003,-8.86570087556951));
#63890=CARTESIAN_POINT('Ctrl Pts',(-20.097255558188,25.4331494754904,-8.87155274565292));
#63891=CARTESIAN_POINT('Ctrl Pts',(-20.0417123150089,25.3312901298539,-8.87740372473591));
#63892=CARTESIAN_POINT('Ctrl Pts',(-19.9906700592396,25.2269528153186,-8.8832547038189));
#63893=CARTESIAN_POINT('Ctrl Pts',(-19.9443442126617,25.1205754904297,-8.88910568290189));
#63894=CARTESIAN_POINT('Ctrl Pts',(-19.8980142009442,25.0141886011957,-8.8949571880442));
#63895=CARTESIAN_POINT('Ctrl Pts',(-19.8564016064521,24.9057617160189,-8.90080869318652));
#63896=CARTESIAN_POINT('Ctrl Pts',(-19.8196738690939,24.7957531708555,-8.90666019832883));
#63897=CARTESIAN_POINT('Ctrl Pts',(-19.7829339352536,24.685708094249,-8.91251364662862));
#63898=CARTESIAN_POINT('Ctrl Pts',(-19.7510822149403,24.574080705159,-8.91836709492842));
#63899=CARTESIAN_POINT('Ctrl Pts',(-19.7242362034355,24.4613442152792,-8.92422054322821));
#63900=CARTESIAN_POINT('Ctrl Pts',(-19.6973596621861,24.3484795195302,-8.93008064816977));
#63901=CARTESIAN_POINT('Ctrl Pts',(-19.6755002877769,24.2345036078746,-8.93594075311132));
#63902=CARTESIAN_POINT('Ctrl Pts',(-19.6587244115379,24.1198996944472,-8.94180085805288));
#63903=CARTESIAN_POINT('Ctrl Pts',(-19.6419372377962,24.0052186024569,-8.94766490940835));
#63904=CARTESIAN_POINT('Ctrl Pts',(-19.6302404205463,23.8899090768447,-8.95352896076382));
#63905=CARTESIAN_POINT('Ctrl Pts',(-19.6236482574694,23.7744575129944,-8.95939301211929));
#63906=CARTESIAN_POINT('Ctrl Pts',(-19.6170463788601,23.6588357965852,-8.96526570591588));
#63907=CARTESIAN_POINT('Ctrl Pts',(-19.6155641746343,23.5430720359407,-8.97113839971246));
#63908=CARTESIAN_POINT('Ctrl Pts',(-19.6191639028281,23.4276507698807,-8.97701109350905));
#63909=CARTESIAN_POINT('Ctrl Pts',(-19.6201494481914,23.3960503579987,-8.97861893883222));
#63910=CARTESIAN_POINT('Ctrl Pts',(-19.6215156229899,23.3644755754901,-8.98022678415538));
#63911=CARTESIAN_POINT('Ctrl Pts',(-19.6232609816518,23.3329362509054,-8.98183462947855));
#63912=CARTESIAN_POINT('Ctrl Pts',(-19.6296355154656,23.2177458918056,-8.98770692644725));
#63913=CARTESIAN_POINT('Ctrl Pts',(-19.6410933399642,23.1026432715625,-8.99357922341594));
#63914=CARTESIAN_POINT('Ctrl Pts',(-19.6576327665207,22.988113435224,-8.99945152038464));
#63915=CARTESIAN_POINT('Ctrl Pts',(-19.6741507592938,22.8737320204576,-9.00531620732283));
#63916=CARTESIAN_POINT('Ctrl Pts',(-19.6957371996832,22.7599223188246,-9.01118089426103));
#63917=CARTESIAN_POINT('Ctrl Pts',(-19.7223384384437,22.6471674334372,-9.01704558119922));
#63918=CARTESIAN_POINT('Ctrl Pts',(-19.7489123194953,22.5345285093909,-9.02290423667403));
#63919=CARTESIAN_POINT('Ctrl Pts',(-19.7804906462226,22.4229426437613,-9.02876289214884));
#63920=CARTESIAN_POINT('Ctrl Pts',(-19.8169683033863,22.3128852173256,-9.03462154762364));
#63921=CARTESIAN_POINT('Ctrl Pts',(-19.8548708099681,22.1985288508756,-9.04070904734155));
#63922=CARTESIAN_POINT('Ctrl Pts',(-19.8980631289842,22.085823212181,-9.04679654705946));
#63923=CARTESIAN_POINT('Ctrl Pts',(-19.9463693817299,21.9752873760785,-9.05288404677736));
#63924=CARTESIAN_POINT('Ctrl Pts',(-19.9928058381377,21.8690300648006,-9.05873591686075));
#63925=CARTESIAN_POINT('Ctrl Pts',(-20.0439675171964,21.7647781199115,-9.06458778694414));
#63926=CARTESIAN_POINT('Ctrl Pts',(-20.0996484940528,21.6629738624424,-9.07043965702752));
#63927=CARTESIAN_POINT('Ctrl Pts',(-20.1553209929741,21.5611851055973,-9.07629063611048));
#63928=CARTESIAN_POINT('Ctrl Pts',(-20.2155112232113,21.4618436577402,-9.08214161519344));
#63929=CARTESIAN_POINT('Ctrl Pts',(-20.2799671674974,21.3653674919907,-9.08799259427639));
#63930=CARTESIAN_POINT('Ctrl Pts',(-20.3444289069932,21.2688826521053,-9.09384409941867));
#63931=CARTESIAN_POINT('Ctrl Pts',(-20.4131568932988,21.1752639501931,-9.09969560456095));
#63932=CARTESIAN_POINT('Ctrl Pts',(-20.4858560290533,21.0849000062727,-9.10554710970324));
#63933=CARTESIAN_POINT('Ctrl Pts',(-20.5585793066083,20.9945060544536,-9.11140055800299));
#63934=CARTESIAN_POINT('Ctrl Pts',(-20.6352760968414,20.9073693317141,-9.11725400630275));
#63935=CARTESIAN_POINT('Ctrl Pts',(-20.7156117899958,20.8238444797872,-9.12310745460251));
#63936=CARTESIAN_POINT('Ctrl Pts',(-20.7960388422778,20.7402246419666,-9.12896755954403));
#63937=CARTESIAN_POINT('Ctrl Pts',(-20.8801127705161,20.6602251714825,-9.13482766448555));
#63938=CARTESIAN_POINT('Ctrl Pts',(-20.9674628934476,20.5841630717207,-9.14068776942708));
#63939=CARTESIAN_POINT('Ctrl Pts',(-21.0548718412199,20.5080497488952,-9.14655182078251));
#63940=CARTESIAN_POINT('Ctrl Pts',(-21.1455610542217,20.4358793333796,-9.15241587213795));
#63941=CARTESIAN_POINT('Ctrl Pts',(-21.2391290483586,20.3679267713776,-9.15827992349339));
#63942=CARTESIAN_POINT('Ctrl Pts',(-21.3328349430408,20.2998740608639,-9.16415261728995));
#63943=CARTESIAN_POINT('Ctrl Pts',(-21.4294277429642,20.2360518373774,-9.1700253110865));
#63944=CARTESIAN_POINT('Ctrl Pts',(-21.5284793963583,20.1766902617436,-9.17589800488306));
#63945=CARTESIAN_POINT('Ctrl Pts',(-21.5555980821281,20.1604380553316,-9.17750585020651));
#63946=CARTESIAN_POINT('Ctrl Pts',(-21.5829009518218,20.1445199326127,-9.17911369552997));
#63947=CARTESIAN_POINT('Ctrl Pts',(-21.6103789551222,20.1289399901514,-9.18072154085343));
#63948=CARTESIAN_POINT('Ctrl Pts',(-21.7107362426876,20.0720377200429,-9.18659383782214));
#63949=CARTESIAN_POINT('Ctrl Pts',(-21.8137674481917,20.0194595342479,-9.19246613479085));
#63950=CARTESIAN_POINT('Ctrl Pts',(-21.9190635823233,19.971466199507,-9.19833843175956));
#63951=CARTESIAN_POINT('Ctrl Pts',(-22.0242232610274,19.9235350603164,-9.20420311869776));
#63952=CARTESIAN_POINT('Ctrl Pts',(-22.1316416586833,19.8801771263302,-9.21006780563596));
#63953=CARTESIAN_POINT('Ctrl Pts',(-22.2408833328458,19.8416083992508,-9.21593249257417));
#63954=CARTESIAN_POINT('Ctrl Pts',(-22.3500126587852,19.8030793376926,-9.22179114804899));
#63955=CARTESIAN_POINT('Ctrl Pts',(-22.4609611440514,19.7693298229638,-9.22764980352382));
#63956=CARTESIAN_POINT('Ctrl Pts',(-22.5732720235775,19.7405283833128,-9.23350845899865));
#63957=CARTESIAN_POINT('Ctrl Pts',(-22.6899698649799,19.7106019340612,-9.23959595871655));
#63958=CARTESIAN_POINT('Ctrl Pts',(-22.8081382892972,19.6860181810953,-9.24568345843445));
#63959=CARTESIAN_POINT('Ctrl Pts',(-22.9272455202642,19.6669097366645,-9.25177095815236));
#63960=CARTESIAN_POINT('Ctrl Pts',(-23.0417424523236,19.6485409252499,-9.25762282823576));
#63961=CARTESIAN_POINT('Ctrl Pts',(-23.1571064191528,19.6352315084791,-9.26347469831916));
#63962=CARTESIAN_POINT('Ctrl Pts',(-23.2728539775337,19.6270473315868,-9.26932656840257));
#63963=CARTESIAN_POINT('Ctrl Pts',(-23.3885839122965,19.6188644008099,-9.27517754748554));
#63964=CARTESIAN_POINT('Ctrl Pts',(-23.5046969102424,19.6158051874455,-9.28102852656851));
#63965=CARTESIAN_POINT('Ctrl Pts',(-23.6207050975568,19.6178835973286,-9.28687950565149));
#63966=CARTESIAN_POINT('Ctrl Pts',(-23.7367237151237,19.6199621940808,-9.29273101079379));
#63967=CARTESIAN_POINT('Ctrl Pts',(-23.8526370899848,19.627179324933,-9.29858251593608));
#63968=CARTESIAN_POINT('Ctrl Pts',(-23.9679587569643,19.639496785119,-9.30443402107838));
#63969=CARTESIAN_POINT('Ctrl Pts',(-24.0833187197589,19.6518183356655,-9.31028746937815));
#63970=CARTESIAN_POINT('Ctrl Pts',(-24.19808617313,19.669243539498,-9.31614091767792));
#63971=CARTESIAN_POINT('Ctrl Pts',(-24.3117818802786,19.6916825827047,-9.32199436597769));
#63972=CARTESIAN_POINT('Ctrl Pts',(-24.4256068841349,19.7141471439762,-9.32785447091923));
#63973=CARTESIAN_POINT('Ctrl Pts',(-24.5383573032639,19.7416368452016,-9.33371457586078));
#63974=CARTESIAN_POINT('Ctrl Pts',(-24.6495660684615,19.7740111797835,-9.33957468080232));
#63975=CARTESIAN_POINT('Ctrl Pts',(-24.7608497258022,19.8064073164536,-9.34543873215777));
#63976=CARTESIAN_POINT('Ctrl Pts',(-24.8705892714847,19.843694503851,-9.35130278351322));
#63977=CARTESIAN_POINT('Ctrl Pts',(-24.9783363694817,19.8856835867499,-9.35716683486867));
#63978=CARTESIAN_POINT('Ctrl Pts',(-25.0862422651928,19.9277345531752,-9.36303952866524));
#63979=CARTESIAN_POINT('Ctrl Pts',(-25.1921494758554,19.9745010789984,-9.36891222246181));
#63980=CARTESIAN_POINT('Ctrl Pts',(-25.2956329831765,20.0257474487665,-9.37478491625838));
#63981=CARTESIAN_POINT('Ctrl Pts',(-25.3239650364131,20.0397778475618,-9.3763927615817));
#63982=CARTESIAN_POINT('Ctrl Pts',(-25.3521155786525,20.0541437897815,-9.37800060690502));
#63983=CARTESIAN_POINT('Ctrl Pts',(-25.3800762713059,20.0688398756086,-9.37960845222834));
#63984=CARTESIAN_POINT('Ctrl Pts',(-25.4821964742451,20.1225140562046,-9.38548074919705));
#63985=CARTESIAN_POINT('Ctrl Pts',(-25.5821241185022,20.1807751997085,-9.39135304616576));
#63986=CARTESIAN_POINT('Ctrl Pts',(-25.6794187405819,20.2434201720287,-9.39722534313448));
#63987=CARTESIAN_POINT('Ctrl Pts',(-25.7765872765583,20.3059839614399,-9.40309003007268));
#63988=CARTESIAN_POINT('Ctrl Pts',(-25.8711292316133,20.3729200602875,-9.40895471701089));
#63989=CARTESIAN_POINT('Ctrl Pts',(-25.962627504789,20.4439788816135,-9.4148194039491));
#63990=CARTESIAN_POINT('Ctrl Pts',(-26.0540316777186,20.51496462339,-9.42067805942392));
#63991=CARTESIAN_POINT('Ctrl Pts',(-26.1423980704441,20.5900644021111,-9.42653671489874));
#63992=CARTESIAN_POINT('Ctrl Pts',(-26.22733799644,20.6689850303249,-9.43239537037356));
#63993=CARTESIAN_POINT('Ctrl Pts',(-26.3155957507595,20.7509883677892,-9.43848287009146));
#63994=CARTESIAN_POINT('Ctrl Pts',(-26.4001535174605,20.8371168851691,-9.44457036980937));
#63995=CARTESIAN_POINT('Ctrl Pts',(-26.4806122800179,20.9269948727129,-9.45065786952727));
#63996=CARTESIAN_POINT('Ctrl Pts',(-26.5579567149051,21.0133939414335,-9.45650973961067));
#63997=CARTESIAN_POINT('Ctrl Pts',(-26.6315132652398,21.1032572783412,-9.46236160969407));
#63998=CARTESIAN_POINT('Ctrl Pts',(-26.7009652127677,21.1962137466861,-9.46821347977748));
#63999=CARTESIAN_POINT('Ctrl Pts',(-26.770406585605,21.2891560615634,-9.47406445886045));
#64000=CARTESIAN_POINT('Ctrl Pts',(-26.8357443509059,21.3851902403952,-9.47991543794342));
#64001=CARTESIAN_POINT('Ctrl Pts',(-26.8967030929787,21.4839133434487,-9.48576641702639));
#64002=CARTESIAN_POINT('Ctrl Pts',(-26.957667315829,21.5826453226593,-9.49161792216869));
#64003=CARTESIAN_POINT('Ctrl Pts',(-27.0142515155815,21.6840663549347,-9.49746942731099));
#64004=CARTESIAN_POINT('Ctrl Pts',(-27.0662248794965,21.7877465176648,-9.50332093245328));
#64005=CARTESIAN_POINT('Ctrl Pts',(-27.1182155026342,21.8914611103199,-9.50917438075306));
#64006=CARTESIAN_POINT('Ctrl Pts',(-27.1655920601704,21.9974359558161,-9.51502782905283));
#64007=CARTESIAN_POINT('Ctrl Pts',(-27.2081710662497,22.1052193159667,-9.52088127735261));
#64008=CARTESIAN_POINT('Ctrl Pts',(-27.2507984939047,22.2131252492026,-9.52674138229415));
#64009=CARTESIAN_POINT('Ctrl Pts',(-27.2886173284035,22.3228434174537,-9.53260148723569));
#64010=CARTESIAN_POINT('Ctrl Pts',(-27.3214933095986,22.4339049177895,-9.53846159217723));
#64011=CARTESIAN_POINT('Ctrl Pts',(-27.3543914307095,22.5450412110949,-9.54432564353268));
#64012=CARTESIAN_POINT('Ctrl Pts',(-27.3823399709694,22.6575222376193,-9.55018969488814));
#64013=CARTESIAN_POINT('Ctrl Pts',(-27.4052557252144,22.7708685583222,-9.55605374624359));
#64014=CARTESIAN_POINT('Ctrl Pts',(-27.4282052527067,22.8843819288756,-9.56192644004016));
#64015=CARTESIAN_POINT('Ctrl Pts',(-27.4461071269598,22.9987627319246,-9.56779913383674));
#64016=CARTESIAN_POINT('Ctrl Pts',(-27.458929918934,23.1135259782533,-9.57367182763331));
#64017=CARTESIAN_POINT('Ctrl Pts',(-27.4624405848774,23.144946235343,-9.57527967295662));
#64018=CARTESIAN_POINT('Ctrl Pts',(-27.4655708381191,23.1763951596308,-9.57688751827993));
#64019=CARTESIAN_POINT('Ctrl Pts',(-27.4683207142553,23.2078628168923,-9.57849536360323));
#64020=CARTESIAN_POINT('Ctrl Pts',(-27.4782068054665,23.3209923232696,-9.5842757350572));
#64021=CARTESIAN_POINT('Ctrl Pts',(-27.4831941018349,23.4345561225121,-9.59005610651116));
#64022=CARTESIAN_POINT('Ctrl Pts',(-27.483252021333,23.5482489098093,-9.59583647796514));
#64023=CARTESIAN_POINT('',(-27.4816334182501,23.5477124661267,-10.8458359655833));
#64024=CARTESIAN_POINT('Ctrl Pts',(-27.4884997658551,23.5482804171771,-9.59583821346848));
#64025=CARTESIAN_POINT('Ctrl Pts',(-27.4810825272021,24.740122181211,-9.65635290063834));
#64026=CARTESIAN_POINT('Ctrl Pts',(-26.2680084891369,27.2507034664838,-9.78316322493322));
#64027=CARTESIAN_POINT('Ctrl Pts',(-21.9924509892916,27.9336308163729,-9.97626918635299));
#64028=CARTESIAN_POINT('Ctrl Pts',(-19.0203850618263,24.6090497443562,-10.1751560977279));
#64029=CARTESIAN_POINT('Ctrl Pts',(-20.2108832697441,20.3115238051025,-10.3740430091028));
#64030=CARTESIAN_POINT('Ctrl Pts',(-24.4699786975713,18.9901149666739,-10.5729299204777));
#64031=CARTESIAN_POINT('Ctrl Pts',(-27.1694554347631,21.2586694379709,-10.7301939012821));
#64032=CARTESIAN_POINT('Ctrl Pts',(-27.481293475824,23.0585648994137,-10.8211622449617));
#64033=CARTESIAN_POINT('Ctrl Pts',(-27.4784306046326,23.5476944236682,-10.8458349515162));
#64034=CARTESIAN_POINT('',(-27.4832514227223,23.5532060332972,-12.0958364780106));
#64035=CARTESIAN_POINT('Ctrl Pts',(-27.4832517173407,23.5477215825155,-10.8458364779652));
#64036=CARTESIAN_POINT('Ctrl Pts',(-27.4833269687236,23.6646593820601,-10.8517278562073));
#64037=CARTESIAN_POINT('Ctrl Pts',(-27.4781826122975,23.781621427634,-10.8576192344494));
#64038=CARTESIAN_POINT('Ctrl Pts',(-27.467838789277,23.8981130129192,-10.8635106126916));
#64039=CARTESIAN_POINT('Ctrl Pts',(-27.4574941529768,24.0146137573178,-10.8694024541414));
#64040=CARTESIAN_POINT('Ctrl Pts',(-27.4419492720751,24.13064356402,-10.8752942955912));
#64041=CARTESIAN_POINT('Ctrl Pts',(-27.4212761986332,24.2457126455741,-10.8811861370411));
#64042=CARTESIAN_POINT('Ctrl Pts',(-27.4005967517939,24.3608172023081,-10.887079794914));
#64043=CARTESIAN_POINT('Ctrl Pts',(-27.3747860381708,24.4749600456985,-10.8929734527869));
#64044=CARTESIAN_POINT('Ctrl Pts',(-27.3439671552581,24.5876619759145,-10.8988671106598));
#64045=CARTESIAN_POINT('Ctrl Pts',(-27.3126633818392,24.7021371078438,-10.9048534967071));
#64046=CARTESIAN_POINT('Ctrl Pts',(-27.2761926203301,24.8151251812877,-10.9108398827545));
#64047=CARTESIAN_POINT('Ctrl Pts',(-27.234735882171,24.9261418586604,-10.9168262688018));
#64048=CARTESIAN_POINT('Ctrl Pts',(-27.1938437091846,25.0356466913384,-10.9227311311879));
#64049=CARTESIAN_POINT('Ctrl Pts',(-27.1481007359123,25.14323313963,-10.9286359935741));
#64050=CARTESIAN_POINT('Ctrl Pts',(-27.0977281388904,25.2484591788217,-10.9345408559603));
#64051=CARTESIAN_POINT('Ctrl Pts',(-27.0463123612841,25.3558643742918,-10.9405680038381));
#64052=CARTESIAN_POINT('Ctrl Pts',(-26.9900733111427,25.4608099245802,-10.946595151716));
#64053=CARTESIAN_POINT('Ctrl Pts',(-26.9292934144627,25.5628557495638,-10.9526222995939));
#64054=CARTESIAN_POINT('Ctrl Pts',(-26.8685135177827,25.6649015745475,-10.9586494474718));
#64055=CARTESIAN_POINT('Ctrl Pts',(-26.803193074387,25.7640473432371,-10.9646765953496));
#64056=CARTESIAN_POINT('Ctrl Pts',(-26.7336580624837,25.8598884827781,-10.9707037432275));
#64057=CARTESIAN_POINT('Ctrl Pts',(-26.6659095605565,25.9532672490881,-10.9765760401962));
#64058=CARTESIAN_POINT('Ctrl Pts',(-26.5939354620773,26.0438190247594,-10.9824483371649));
#64059=CARTESIAN_POINT('Ctrl Pts',(-26.5179998988967,26.1311369856097,-10.9883206341336));
#64060=CARTESIAN_POINT('Ctrl Pts',(-26.4421627421755,26.2183417893172,-10.9941853210718));
#64061=CARTESIAN_POINT('Ctrl Pts',(-26.3623745986895,26.3023208030858,-11.00005000801));
#64062=CARTESIAN_POINT('Ctrl Pts',(-26.2789422276475,26.3826969783159,-11.0059146949482));
#64063=CARTESIAN_POINT('Ctrl Pts',(-26.195595661576,26.4629904916816,-11.011773350423));
#64064=CARTESIAN_POINT('Ctrl Pts',(-26.1086126185523,26.5396882514509,-11.0176320058978));
#64065=CARTESIAN_POINT('Ctrl Pts',(-26.018338938545,26.6124475758281,-11.0234906613727));
#64066=CARTESIAN_POINT('Ctrl Pts',(-25.9245390890847,26.688048943501,-11.0295781610906));
#64067=CARTESIAN_POINT('Ctrl Pts',(-25.8271865899897,26.7593975828396,-11.0356656608085));
#64068=CARTESIAN_POINT('Ctrl Pts',(-25.7267104322242,26.8261524091661,-11.0417531605264));
#64069=CARTESIAN_POINT('Ctrl Pts',(-25.6301234180198,26.8903233478445,-11.0476050306098));
#64070=CARTESIAN_POINT('Ctrl Pts',(-25.5306504409234,26.950249237449,-11.0534569006932));
#64071=CARTESIAN_POINT('Ctrl Pts',(-25.4287041775526,27.0056697878547,-11.0593087707766));
#64072=CARTESIAN_POINT('Ctrl Pts',(-25.3267734364273,27.0610818999778,-11.0651597498595));
#64073=CARTESIAN_POINT('Ctrl Pts',(-25.2223705208762,27.1119898394649,-11.0710107289425));
#64074=CARTESIAN_POINT('Ctrl Pts',(-25.115933666313,27.1581787483315,-11.0768617080255));
#64075=CARTESIAN_POINT('Ctrl Pts',(-25.0094872420524,27.2043718100255,-11.0827132131677));
#64076=CARTESIAN_POINT('Ctrl Pts',(-24.9010068944877,27.2458448330844,-11.08856471831));
#64077=CARTESIAN_POINT('Ctrl Pts',(-24.7909511746775,27.2824309675811,-11.0944162234523));
#64078=CARTESIAN_POINT('Ctrl Pts',(-24.6808589077582,27.3190292515368,-11.1002696717521));
#64079=CARTESIAN_POINT('Ctrl Pts',(-24.5691906204166,27.3507372897001,-11.1061231200519));
#64080=CARTESIAN_POINT('Ctrl Pts',(-24.4564196751618,27.3774381958735,-11.1119765683517));
#64081=CARTESIAN_POINT('Ctrl Pts',(-24.343520484855,27.4041694667752,-11.1178366732932));
#64082=CARTESIAN_POINT('Ctrl Pts',(-24.2295165362655,27.4258821449429,-11.1236967782348));
#64083=CARTESIAN_POINT('Ctrl Pts',(-24.1148911284914,27.4425105209604,-11.1295568831763));
#64084=CARTESIAN_POINT('Ctrl Pts',(-24.000188527679,27.4591500951486,-11.1354209345318));
#64085=CARTESIAN_POINT('Ctrl Pts',(-23.8848640446584,27.4706985083149,-11.1412849858872));
#64086=CARTESIAN_POINT('Ctrl Pts',(-23.7694040928103,27.4771420887432,-11.1471490372427));
#64087=CARTESIAN_POINT('Ctrl Pts',(-23.6537739760415,27.4835951657228,-11.1530217310392));
#64088=CARTESIAN_POINT('Ctrl Pts',(-23.5380084037779,27.4849283897584,-11.1588944248358));
#64089=CARTESIAN_POINT('Ctrl Pts',(-23.4225918658673,27.4811801263467,-11.1647671186324));
#64090=CARTESIAN_POINT('Ctrl Pts',(-23.3909927484701,27.4801539145254,-11.1663749639557));
#64091=CARTESIAN_POINT('Ctrl Pts',(-23.3594197502655,27.4787471065669,-11.167982809279));
#64092=CARTESIAN_POINT('Ctrl Pts',(-23.3278826979357,27.4769611606905,-11.1695906546024));
#64093=CARTESIAN_POINT('Ctrl Pts',(-23.2127006377526,27.4704383911156,-11.1754629515711));
#64094=CARTESIAN_POINT('Ctrl Pts',(-23.0976128581538,27.4588324479783,-11.1813352485398));
#64095=CARTESIAN_POINT('Ctrl Pts',(-22.9831044016121,27.4421456441196,-11.1872075455085));
#64096=CARTESIAN_POINT('Ctrl Pts',(-22.8687443389359,27.4254804650334,-11.1930722324467));
#64097=CARTESIAN_POINT('Ctrl Pts',(-22.7549625116179,27.4037475782785,-11.1989369193849));
#64098=CARTESIAN_POINT('Ctrl Pts',(-22.6422419533278,27.3770012547716,-11.2048016063231));
#64099=CARTESIAN_POINT('Ctrl Pts',(-22.5296373210751,27.3502824381841,-11.2106602617979));
#64100=CARTESIAN_POINT('Ctrl Pts',(-22.4180921866996,27.3185605352692,-11.2165189172728));
#64101=CARTESIAN_POINT('Ctrl Pts',(-22.30808179531,27.2819412729574,-11.2223775727476));
#64102=CARTESIAN_POINT('Ctrl Pts',(-22.1937743011372,27.243891630006,-11.2284650724655));
#64103=CARTESIAN_POINT('Ctrl Pts',(-22.0811243409304,27.2005543033591,-11.2345525721834));
#64104=CARTESIAN_POINT('Ctrl Pts',(-21.9706507627541,27.1521058395847,-11.2406400719013));
#64105=CARTESIAN_POINT('Ctrl Pts',(-21.8644532995766,27.1055326767285,-11.2464919419847));
#64106=CARTESIAN_POINT('Ctrl Pts',(-21.7602672821216,27.0542368758851,-11.2523438120681));
#64107=CARTESIAN_POINT('Ctrl Pts',(-21.6585347660448,26.9984249309699,-11.2581956821515));
#64108=CARTESIAN_POINT('Ctrl Pts',(-21.5568177396686,26.9426214839307,-11.2640466612345));
#64109=CARTESIAN_POINT('Ctrl Pts',(-21.457553834223,26.8823034588131,-11.2698976403174));
#64110=CARTESIAN_POINT('Ctrl Pts',(-21.3611606981547,26.8177234105745,-11.2757486194004));
#64111=CARTESIAN_POINT('Ctrl Pts',(-21.2647588954157,26.7531375559679,-11.2816001245427));
#64112=CARTESIAN_POINT('Ctrl Pts',(-21.1712287186044,26.6842891465812,-11.287451629685));
#64113=CARTESIAN_POINT('Ctrl Pts',(-21.0809584076506,26.6114737796545,-11.2933031348273));
#64114=CARTESIAN_POINT('Ctrl Pts',(-20.9906581198916,26.5386342323296,-11.2991565831271));
#64115=CARTESIAN_POINT('Ctrl Pts',(-20.9036201721168,26.4618253674175,-11.3050100314268));
#64116=CARTESIAN_POINT('Ctrl Pts',(-20.820198775149,26.3813822507946,-11.3108634797266));
#64117=CARTESIAN_POINT('Ctrl Pts',(-20.7366825099383,26.3008476528803,-11.3167235846682));
#64118=CARTESIAN_POINT('Ctrl Pts',(-20.6567913023122,26.2166708411609,-11.3225836896097));
#64119=CARTESIAN_POINT('Ctrl Pts',(-20.5808416783557,26.1292229045515,-11.3284437945512));
#64120=CARTESIAN_POINT('Ctrl Pts',(-20.5048409070811,26.04171607723,-11.3343078459067));
#64121=CARTESIAN_POINT('Ctrl Pts',(-20.4327872612978,25.9509340616106,-11.3401718972621));
#64122=CARTESIAN_POINT('Ctrl Pts',(-20.3649551703029,25.8572786952896,-11.3460359486175));
#64123=CARTESIAN_POINT('Ctrl Pts',(-20.2970231083467,25.7634852996543,-11.3519086424141));
#64124=CARTESIAN_POINT('Ctrl Pts',(-20.2333252451369,25.6668104454763,-11.3577813362107));
#64125=CARTESIAN_POINT('Ctrl Pts',(-20.1740911904395,25.5676824803709,-11.3636540300072));
#64126=CARTESIAN_POINT('Ctrl Pts',(-20.1578738971279,25.540542901733,-11.3652618753306));
#64127=CARTESIAN_POINT('Ctrl Pts',(-20.1419909242631,25.5132195692635,-11.3668697206539));
#64128=CARTESIAN_POINT('Ctrl Pts',(-20.1264463567591,25.485721538544,-11.3684775659772));
#64129=CARTESIAN_POINT('Ctrl Pts',(-20.0696732858,25.3852911052837,-11.374349862946));
#64130=CARTESIAN_POINT('Ctrl Pts',(-20.0172277366982,25.2821923210592,-11.3802221599147));
#64131=CARTESIAN_POINT('Ctrl Pts',(-19.9693699496409,25.1768345104299,-11.3860944568834));
#64132=CARTESIAN_POINT('Ctrl Pts',(-19.9215741824751,25.0716132351559,-11.3919591438216));
#64133=CARTESIAN_POINT('Ctrl Pts',(-19.8783545235224,24.9641391281602,-11.3978238307598));
#64134=CARTESIAN_POINT('Ctrl Pts',(-19.8399264139257,24.8548479095048,-11.403688517698));
#64135=CARTESIAN_POINT('Ctrl Pts',(-19.8015378252342,24.7456690900264,-11.4095471731728));
#64136=CARTESIAN_POINT('Ctrl Pts',(-19.7679311205307,24.6346772636328,-11.4154058286476));
#64137=CARTESIAN_POINT('Ctrl Pts',(-19.7392742401032,24.5223294118957,-11.4212644841224));
#64138=CARTESIAN_POINT('Ctrl Pts',(-19.7094979966855,24.4055931541146,-11.4273519838403));
#64139=CARTESIAN_POINT('Ctrl Pts',(-19.6850663376552,24.2873931902714,-11.4334394835582));
#64140=CARTESIAN_POINT('Ctrl Pts',(-19.6661111907973,24.1682614668524,-11.4395269832761));
#64141=CARTESIAN_POINT('Ctrl Pts',(-19.6478897432466,24.0537409903734,-11.4453788533595));
#64142=CARTESIAN_POINT('Ctrl Pts',(-19.6347288019565,23.9383599908905,-11.4512307234429));
#64143=CARTESIAN_POINT('Ctrl Pts',(-19.6266935899533,23.8226019959587,-11.4570825935263));
#64144=CARTESIAN_POINT('Ctrl Pts',(-19.6186596013842,23.7068616262343,-11.4629335726092));
#64145=CARTESIAN_POINT('Ctrl Pts',(-19.6157498189573,23.59074478747,-11.4687845516922));
#64146=CARTESIAN_POINT('Ctrl Pts',(-19.6179775206404,23.4747393709723,-11.4746355307752));
#64147=CARTESIAN_POINT('Ctrl Pts',(-19.6202054226154,23.3587235244714,-11.4804870359175));
#64148=CARTESIAN_POINT('Ctrl Pts',(-19.6275717189959,23.2428195334831,-11.4863385410597));
#64149=CARTESIAN_POINT('Ctrl Pts',(-19.6400375790048,23.1275138136139,-11.492190046202));
#64150=CARTESIAN_POINT('Ctrl Pts',(-19.6525075786544,23.0121698032251,-11.4980434945018));
#64151=CARTESIAN_POINT('Ctrl Pts',(-19.6700804648502,22.8974248697742,-11.5038969428016));
#64152=CARTESIAN_POINT('Ctrl Pts',(-19.6926658070144,22.78375813408,-11.5097503911013));
#64153=CARTESIAN_POINT('Ctrl Pts',(-19.7152768336169,22.6699621346249,-11.5156104960429));
#64154=CARTESIAN_POINT('Ctrl Pts',(-19.7429116131051,22.5572471859717,-11.5214706009844));
#64155=CARTESIAN_POINT('Ctrl Pts',(-19.7754290379162,22.4460801761168,-11.527330705926));
#64156=CARTESIAN_POINT('Ctrl Pts',(-19.8079683611775,22.3348383022388,-11.5331947572814));
#64157=CARTESIAN_POINT('Ctrl Pts',(-19.8453967439644,22.2251468331425,-11.5390588086368));
#64158=CARTESIAN_POINT('Ctrl Pts',(-19.8875244542338,22.1174538610558,-11.5449228599923));
#64159=CARTESIAN_POINT('Ctrl Pts',(-19.9297142523388,22.0096021710255,-11.5507955537888));
#64160=CARTESIAN_POINT('Ctrl Pts',(-19.9766170337844,21.9037552329472,-11.5566682475854));
#64161=CARTESIAN_POINT('Ctrl Pts',(-20.0279965363475,21.8003377614141,-11.562540941382));
#64162=CARTESIAN_POINT('Ctrl Pts',(-20.0420633846754,21.772023787671,-11.5641487867053));
#64163=CARTESIAN_POINT('Ctrl Pts',(-20.0564655425593,21.7438917565931,-11.5657566320287));
#64164=CARTESIAN_POINT('Ctrl Pts',(-20.0711975994555,21.715949999813,-11.5673644773521));
#64165=CARTESIAN_POINT('Ctrl Pts',(-20.1250031563694,21.613898955937,-11.5732367743208));
#64166=CARTESIAN_POINT('Ctrl Pts',(-20.1833928507401,21.5140463719922,-11.5791090712895));
#64167=CARTESIAN_POINT('Ctrl Pts',(-20.246162981802,21.4168324496913,-11.5849813682582));
#64168=CARTESIAN_POINT('Ctrl Pts',(-20.3088517677592,21.3197445089131,-11.5908460551964));
#64169=CARTESIAN_POINT('Ctrl Pts',(-20.3759094793266,21.2252887737039,-11.5967107421346));
#64170=CARTESIAN_POINT('Ctrl Pts',(-20.4470859929765,21.1338820234768,-11.6025754290728));
#64171=CARTESIAN_POINT('Ctrl Pts',(-20.5181893060374,21.0425692793706,-11.6084340845477));
#64172=CARTESIAN_POINT('Ctrl Pts',(-20.5934027432491,20.9542996073988,-11.6142927400225));
#64173=CARTESIAN_POINT('Ctrl Pts',(-20.6724326171932,20.8694613164554,-11.6201513954973));
#64174=CARTESIAN_POINT('Ctrl Pts',(-20.7545494676223,20.7813091671431,-11.6262388952152));
#64175=CARTESIAN_POINT('Ctrl Pts',(-20.8407867329545,20.6968623111711,-11.6323263949331));
#64176=CARTESIAN_POINT('Ctrl Pts',(-20.930768190246,20.6165192812252,-11.638413894651));
#64177=CARTESIAN_POINT('Ctrl Pts',(-21.0172667236974,20.5392860992724,-11.6442657647344));
#64178=CARTESIAN_POINT('Ctrl Pts',(-21.1072246477542,20.4658452569793,-11.6501176348178));
#64179=CARTESIAN_POINT('Ctrl Pts',(-21.200270418382,20.3965129947139,-11.6559695049012));
#64180=CARTESIAN_POINT('Ctrl Pts',(-21.2933020219452,20.3271912889158,-11.6618204839842));
#64181=CARTESIAN_POINT('Ctrl Pts',(-21.3894202058785,20.2619771662448,-11.6676714630671));
#64182=CARTESIAN_POINT('Ctrl Pts',(-21.4882216763444,20.201145523612,-11.6735224421501));
#64183=CARTESIAN_POINT('Ctrl Pts',(-21.5870320300134,20.1403084116291,-11.6793739472924));
#64184=CARTESIAN_POINT('Ctrl Pts',(-21.6885257977711,20.0838547797193,-11.6852254524347));
#64185=CARTESIAN_POINT('Ctrl Pts',(-21.7922727603254,20.0320148871542,-11.691076957577));
#64186=CARTESIAN_POINT('Ctrl Pts',(-21.8960541749875,19.9801577796893,-11.6969304058768));
#64187=CARTESIAN_POINT('Ctrl Pts',(-22.0020899026752,19.9329176427749,-11.7027838541766));
#64188=CARTESIAN_POINT('Ctrl Pts',(-22.1099279694438,19.8904773807623,-11.7086373024764));
#64189=CARTESIAN_POINT('Ctrl Pts',(-22.217888671511,19.8479888549562,-11.7144974074179));
#64190=CARTESIAN_POINT('Ctrl Pts',(-22.327655418807,19.81031125053,-11.7203575123595));
#64191=CARTESIAN_POINT('Ctrl Pts',(-22.4387591360074,19.7775782240784,-11.726217617301));
#64192=CARTESIAN_POINT('Ctrl Pts',(-22.5499376746075,19.7448231539821,-11.7320816686565));
#64193=CARTESIAN_POINT('Ctrl Pts',(-22.6624545755873,19.7170193912054,-11.7379457200119));
#64194=CARTESIAN_POINT('Ctrl Pts',(-22.7758302932245,19.6942495238422,-11.7438097713674));
#64195=CARTESIAN_POINT('Ctrl Pts',(-22.8893731040377,19.6714460982398,-11.749682465164));
#64196=CARTESIAN_POINT('Ctrl Pts',(-23.0037768506907,19.6536914380151,-11.7555551589606));
#64197=CARTESIAN_POINT('Ctrl Pts',(-23.1185565039226,19.6410163480381,-11.7614278527571));
#64198=CARTESIAN_POINT('Ctrl Pts',(-23.1499812529472,19.6375461204309,-11.7630356980804));
#64199=CARTESIAN_POINT('Ctrl Pts',(-23.1814341795848,19.6344563421027,-11.7646435434037));
#64200=CARTESIAN_POINT('Ctrl Pts',(-23.2129053496646,19.6317469646729,-11.766251388727));
#64201=CARTESIAN_POINT('Ctrl Pts',(-23.3278467896063,19.6218515670017,-11.7721236856957));
#64202=CARTESIAN_POINT('Ctrl Pts',(-23.4434165489523,19.6170012418788,-11.7779959826644));
#64203=CARTESIAN_POINT('Ctrl Pts',(-23.5591341697166,19.6172625601196,-11.7838682796331));
#64204=CARTESIAN_POINT('Ctrl Pts',(-23.6747018296348,19.6175235397128,-11.7897329665713));
#64205=CARTESIAN_POINT('Ctrl Pts',(-23.7904165603483,19.6228829884219,-11.7955976535095));
#64206=CARTESIAN_POINT('Ctrl Pts',(-23.9057925159736,19.6333557600676,-11.8014623404477));
#64207=CARTESIAN_POINT('Ctrl Pts',(-24.0210498146512,19.6438177611234,-11.8073209959226));
#64208=CARTESIAN_POINT('Ctrl Pts',(-24.1359686220287,19.6593825880814,-11.8131796513974));
#64209=CARTESIAN_POINT('Ctrl Pts',(-24.2500634968185,19.6800130542081,-11.8190383068722));
#64210=CARTESIAN_POINT('Ctrl Pts',(-24.3686150179109,19.7014493645127,-11.8251258065901));
#64211=CARTESIAN_POINT('Ctrl Pts',(-24.4862764724795,19.7283551171377,-11.831213306308));
#64212=CARTESIAN_POINT('Ctrl Pts',(-24.602509203839,19.7606292132196,-11.8373008060259));
#64213=CARTESIAN_POINT('Ctrl Pts',(-24.7142428999168,19.7916540717136,-11.8431526761093));
#64214=CARTESIAN_POINT('Ctrl Pts',(-24.8246559842864,19.8276392939211,-11.8490045461927));
#64215=CARTESIAN_POINT('Ctrl Pts',(-24.9332815633186,19.8684432349375,-11.8548564162761));
#64216=CARTESIAN_POINT('Ctrl Pts',(-25.0418906031188,19.9092409631829,-11.8607073953591));
#64217=CARTESIAN_POINT('Ctrl Pts',(-25.1487122918557,19.9548558060941,-11.8665583744421));
#64218=CARTESIAN_POINT('Ctrl Pts',(-25.2532973567295,20.0050970592332,-11.872409353525));
#64219=CARTESIAN_POINT('Ctrl Pts',(-25.357891824807,20.0553428295443,-11.8782608586673));
#64220=CARTESIAN_POINT('Ctrl Pts',(-25.4602488966248,20.1102156579598,-11.8841123638096));
#64221=CARTESIAN_POINT('Ctrl Pts',(-25.5599422994288,20.1694780586684,-11.8899638689519));
#64222=CARTESIAN_POINT('Ctrl Pts',(-25.6596688082408,20.2287601391297,-11.8958173172517));
#64223=CARTESIAN_POINT('Ctrl Pts',(-25.7567295340216,20.2924344792726,-11.9016707655514));
#64224=CARTESIAN_POINT('Ctrl Pts',(-25.8507262851938,20.3602196933899,-11.9075242138511));
#64225=CARTESIAN_POINT('Ctrl Pts',(-25.9448299310837,20.4280819940155,-11.9133843187927));
#64226=CARTESIAN_POINT('Ctrl Pts',(-26.0358623121079,20.5000642577497,-11.9192444237342));
#64227=CARTESIAN_POINT('Ctrl Pts',(-26.1234574256321,20.5758440907073,-11.9251045286757));
#64228=CARTESIAN_POINT('Ctrl Pts',(-26.2111115289827,20.6516749566393,-11.9309685800312));
#64229=CARTESIAN_POINT('Ctrl Pts',(-26.2953234560146,20.7313082008036,-11.9368326313866));
#64230=CARTESIAN_POINT('Ctrl Pts',(-26.3757645091863,20.8143850157043,-11.9426966827421));
#64231=CARTESIAN_POINT('Ctrl Pts',(-26.4563241164129,20.8975842692466,-11.9485693765386));
#64232=CARTESIAN_POINT('Ctrl Pts',(-26.533101484937,20.9842369142749,-11.9544420703352));
#64233=CARTESIAN_POINT('Ctrl Pts',(-26.6058085192272,21.0739515388722,-11.9603147641318));
#64234=CARTESIAN_POINT('Ctrl Pts',(-26.6257144889762,21.0985139023452,-11.9619226094551));
#64235=CARTESIAN_POINT('Ctrl Pts',(-26.6453156115578,21.1233056210805,-11.9635304547785));
#64236=CARTESIAN_POINT('Ctrl Pts',(-26.664606557835,21.1483183111418,-11.9651383001019));
#64237=CARTESIAN_POINT('Ctrl Pts',(-26.7351444391807,21.2397779076973,-11.9710174312245));
#64238=CARTESIAN_POINT('Ctrl Pts',(-26.8017714608122,21.3345047763228,-11.9768965623471));
#64239=CARTESIAN_POINT('Ctrl Pts',(-26.8641701381952,21.4321309352501,-11.9827756934698));
#64240=CARTESIAN_POINT('Ctrl Pts',(-26.9264889862588,21.5296321968215,-11.9886473031664));
#64241=CARTESIAN_POINT('Ctrl Pts',(-26.9845900250466,21.630025031603,-11.9945189128629));
#64242=CARTESIAN_POINT('Ctrl Pts',(-27.0381961265906,21.732908734054,-12.0003905225595));
#64243=CARTESIAN_POINT('Ctrl Pts',(-27.0917465023943,21.8356854846784,-12.0062560284771));
#64244=CARTESIAN_POINT('Ctrl Pts',(-27.1408110437252,21.9409475915276,-12.0121215343947));
#64245=CARTESIAN_POINT('Ctrl Pts',(-27.1851564316397,22.0482663006784,-12.0179870403123));
#64246=CARTESIAN_POINT('Ctrl Pts',(-27.2294663524372,22.1554991771106,-12.0238478550412));
#64247=CARTESIAN_POINT('Ctrl Pts',(-27.2690644708402,22.2647850052192,-12.02970866977));
#64248=CARTESIAN_POINT('Ctrl Pts',(-27.3037641718483,22.3756720247779,-12.0355694844989));
#64249=CARTESIAN_POINT('Ctrl Pts',(-27.338445871842,22.4865015199552,-12.0414272588381));
#64250=CARTESIAN_POINT('Ctrl Pts',(-27.3682340864401,22.5989301623155,-12.0472850331774));
#64251=CARTESIAN_POINT('Ctrl Pts',(-27.3929911871134,22.7124884681613,-12.0531428075167));
#64252=CARTESIAN_POINT('Ctrl Pts',(-27.417740802691,22.8260124406337,-12.0589988108084));
#64253=CARTESIAN_POINT('Ctrl Pts',(-27.437462245683,22.9406649946853,-12.0648548141001));
#64254=CARTESIAN_POINT('Ctrl Pts',(-27.4520685658512,23.0559645229432,-12.0707108173919));
#64255=CARTESIAN_POINT('Ctrl Pts',(-27.4666766293965,23.1712778130894,-12.0765675196428));
#64256=CARTESIAN_POINT('Ctrl Pts',(-27.4761682968273,23.287237823602,-12.0824242218937));
#64257=CARTESIAN_POINT('Ctrl Pts',(-27.4805083110525,23.4033562797998,-12.0882809241447));
#64258=CARTESIAN_POINT('Ctrl Pts',(-27.4823746179294,23.4532899118315,-12.0907994420848));
#64259=CARTESIAN_POINT('Ctrl Pts',(-27.483288935297,23.5032527983013,-12.093317960025));
#64260=CARTESIAN_POINT('Ctrl Pts',(-27.483251422723,23.5532060323939,-12.0958364779651));
#64261=CARTESIAN_POINT('',(-27.48469778642,23.5516324603682,-13.3458364779651));
#64262=CARTESIAN_POINT('Ctrl Pts',(-27.4832514227223,23.5532060332972,-12.0958364780106));
#64263=CARTESIAN_POINT('Ctrl Pts',(-27.4831507123894,23.6873158733359,-12.102597962912));
#64264=CARTESIAN_POINT('Ctrl Pts',(-27.4761866223843,23.8211447706251,-12.1093594478134));
#64265=CARTESIAN_POINT('Ctrl Pts',(-27.4624688174035,23.9540504190472,-12.1161209327148));
#64266=CARTESIAN_POINT('Ctrl Pts',(-27.4486733708594,24.0877083016881,-12.1229206870228));
#64267=CARTESIAN_POINT('Ctrl Pts',(-27.4280476574859,24.2204323263878,-12.1297204413309));
#64268=CARTESIAN_POINT('Ctrl Pts',(-27.4007524368963,24.3515885910592,-12.136520195639));
#64269=CARTESIAN_POINT('Ctrl Pts',(-27.3732778581082,24.4836066898115,-12.1433646314574));
#64270=CARTESIAN_POINT('Ctrl Pts',(-27.3390459221007,24.6140362322264,-12.1502090672759));
#64271=CARTESIAN_POINT('Ctrl Pts',(-27.2982687712955,24.7422522245149,-12.1570535030943));
#64272=CARTESIAN_POINT('Ctrl Pts',(-27.2844236367647,24.7857856158181,-12.1593774058885));
#64273=CARTESIAN_POINT('Ctrl Pts',(-27.2698243598901,24.8290640152035,-12.1617013086826));
#64274=CARTESIAN_POINT('Ctrl Pts',(-27.2544804696585,24.8720635558593,-12.1640252114768));
#64275=CARTESIAN_POINT('Ctrl Pts',(-27.2157078151732,24.9807195946939,-12.1698975084455));
#64276=CARTESIAN_POINT('Ctrl Pts',(-27.1720853447534,25.0878502392532,-12.1757698054142));
#64277=CARTESIAN_POINT('Ctrl Pts',(-27.1237522016443,25.1929908276094,-12.181642102383));
#64278=CARTESIAN_POINT('Ctrl Pts',(-27.0754816944502,25.2979951621133,-12.1875067893212));
#64279=CARTESIAN_POINT('Ctrl Pts',(-27.022512825608,25.4010141968992,-12.1933714762594));
#64280=CARTESIAN_POINT('Ctrl Pts',(-26.9650340161279,25.5015998645821,-12.1992361631976));
#64281=CARTESIAN_POINT('Ctrl Pts',(-26.9076143200052,25.6020820862025,-12.2050948186725));
#64282=CARTESIAN_POINT('Ctrl Pts',(-26.845694112712,25.7001355616948,-12.2109534741473));
#64283=CARTESIAN_POINT('Ctrl Pts',(-26.7795089797908,25.7953342211715,-12.2168121296222));
#64284=CARTESIAN_POINT('Ctrl Pts',(-26.7107385972829,25.8942514241368,-12.2228996293401));
#64285=CARTESIAN_POINT('Ctrl Pts',(-26.6373635032458,25.9900858281394,-12.228987129058));
#64286=CARTESIAN_POINT('Ctrl Pts',(-26.559699531327,26.0823895256978,-12.2350746287759));
#64287=CARTESIAN_POINT('Ctrl Pts',(-26.4850417087573,26.1711204121637,-12.2409264988593));
#64288=CARTESIAN_POINT('Ctrl Pts',(-26.4064211459179,26.256588491095,-12.2467783689427));
#64289=CARTESIAN_POINT('Ctrl Pts',(-26.324160727766,26.3384279780687,-12.2526302390261));
#64290=CARTESIAN_POINT('Ctrl Pts',(-26.2419128345107,26.4202550042363,-12.2584812181091));
#64291=CARTESIAN_POINT('Ctrl Pts',(-26.1560264808464,26.4984542454905,-12.2643321971921));
#64292=CARTESIAN_POINT('Ctrl Pts',(-26.0668618493745,26.572696334673,-12.2701831762751));
#64293=CARTESIAN_POINT('Ctrl Pts',(-25.9776892011441,26.6469450989337,-12.2760346814174));
#64294=CARTESIAN_POINT('Ctrl Pts',(-25.8852380068696,26.7172357393258,-12.2818861865597));
#64295=CARTESIAN_POINT('Ctrl Pts',(-25.7899014389786,26.7832792516735,-12.287737691702));
#64296=CARTESIAN_POINT('Ctrl Pts',(-25.694533211889,26.8493446956338,-12.2935911400018));
#64297=CARTESIAN_POINT('Ctrl Pts',(-25.5962780455541,26.9111599718238,-12.2994445883016));
#64298=CARTESIAN_POINT('Ctrl Pts',(-25.4955573695643,26.9684798628937,-12.3052980366013));
#64299=CARTESIAN_POINT('Ctrl Pts',(-25.3947221522947,27.0258649391266,-12.3111581415429));
#64300=CARTESIAN_POINT('Ctrl Pts',(-25.2914161885206,27.0787442217997,-12.3170182464845));
#64301=CARTESIAN_POINT('Ctrl Pts',(-25.1860848275753,27.1269188146667,-12.322878351426));
#64302=CARTESIAN_POINT('Ctrl Pts',(-25.080682532551,27.1751258501068,-12.3287424027815));
#64303=CARTESIAN_POINT('Ctrl Pts',(-24.9732525066363,27.2186217322415,-12.334606454137));
#64304=CARTESIAN_POINT('Ctrl Pts',(-24.8642577135746,27.2572566296136,-12.3404705054924));
#64305=CARTESIAN_POINT('Ctrl Pts',(-24.7551022839451,27.2959484671123,-12.346343199289));
#64306=CARTESIAN_POINT('Ctrl Pts',(-24.6443778784001,27.3297649013522,-12.3522158930856));
#64307=CARTESIAN_POINT('Ctrl Pts',(-24.5325602402114,27.3586065811213,-12.3580885868822));
#64308=CARTESIAN_POINT('Ctrl Pts',(-24.5019464413595,27.3665029505788,-12.3596964322053));
#64309=CARTESIAN_POINT('Ctrl Pts',(-24.4712507388927,27.3740267245054,-12.3613042775285));
#64310=CARTESIAN_POINT('Ctrl Pts',(-24.4404829732302,27.3811765404632,-12.3629121228517));
#64311=CARTESIAN_POINT('Ctrl Pts',(-24.3281105612624,27.4072896509539,-12.3687844198204));
#64312=CARTESIAN_POINT('Ctrl Pts',(-24.2143999579809,27.4284979896557,-12.3746567167891));
#64313=CARTESIAN_POINT('Ctrl Pts',(-24.0998173040847,27.4446674506451,-12.3805290137578));
#64314=CARTESIAN_POINT('Ctrl Pts',(-23.985383140208,27.4608159572972,-12.386393700696));
#64315=CARTESIAN_POINT('Ctrl Pts',(-23.8700795786453,27.4719385148041,-12.3922583876342));
#64316=CARTESIAN_POINT('Ctrl Pts',(-23.7543854355493,27.4779514455067,-12.3981230745724));
#64317=CARTESIAN_POINT('Ctrl Pts',(-23.6388102766371,27.4839581922864,-12.4039817300472));
#64318=CARTESIAN_POINT('Ctrl Pts',(-23.5228457455147,27.4848657432637,-12.409840385522));
#64319=CARTESIAN_POINT('Ctrl Pts',(-23.4069776459001,27.4806419916715,-12.4156990409968));
#64320=CARTESIAN_POINT('Ctrl Pts',(-23.2865836362589,27.4762532566219,-12.4217865407147));
#64321=CARTESIAN_POINT('Ctrl Pts',(-23.1662941953199,27.4663241169753,-12.4278740404326));
#64322=CARTESIAN_POINT('Ctrl Pts',(-23.046656876638,27.4508781758965,-12.4339615401505));
#64323=CARTESIAN_POINT('Ctrl Pts',(-22.9316503750372,27.4360301028456,-12.4398134102339));
#64324=CARTESIAN_POINT('Ctrl Pts',(-22.8172468990511,27.4160844241251,-12.4456652803173));
#64325=CARTESIAN_POINT('Ctrl Pts',(-22.7039287222596,27.3911150662799,-12.4515171504007));
#64326=CARTESIAN_POINT('Ctrl Pts',(-22.590627799191,27.3661495102465,-12.4573681294837));
#64327=CARTESIAN_POINT('Ctrl Pts',(-22.4784122503415,27.3361618848855,-12.4632191085667));
#64328=CARTESIAN_POINT('Ctrl Pts',(-22.3677538717931,27.301277180951,-12.4690700876496));
#64329=CARTESIAN_POINT('Ctrl Pts',(-22.2570855439913,27.2663893405458,-12.4749215927919));
#64330=CARTESIAN_POINT('Ctrl Pts',(-22.1479750590864,27.2266036705977,-12.4807730979342));
#64331=CARTESIAN_POINT('Ctrl Pts',(-22.0408780875052,27.182094734658,-12.4866246030765));
#64332=CARTESIAN_POINT('Ctrl Pts',(-21.9337455513511,27.1375710182696,-12.4924780513763));
#64333=CARTESIAN_POINT('Ctrl Pts',(-21.8286282396043,27.0883210755992,-12.4983314996761));
#64334=CARTESIAN_POINT('Ctrl Pts',(-21.725960258295,27.0345669120589,-12.5041849479758));
#64335=CARTESIAN_POINT('Ctrl Pts',(-21.6231755211971,26.9807516183621,-12.5100450529174));
#64336=CARTESIAN_POINT('Ctrl Pts',(-21.5228460405923,26.9224220717432,-12.5159051578589));
#64337=CARTESIAN_POINT('Ctrl Pts',(-21.425379881424,26.8598454402154,-12.5217652628004));
#64338=CARTESIAN_POINT('Ctrl Pts',(-21.3278480848978,26.7972266672428,-12.5276293141559));
#64339=CARTESIAN_POINT('Ctrl Pts',(-21.2331837861844,26.7303553521689,-12.5334933655113));
#64340=CARTESIAN_POINT('Ctrl Pts',(-21.1417632925323,26.6595400039041,-12.5393574168668));
#64341=CARTESIAN_POINT('Ctrl Pts',(-21.0502080633219,26.5886202879521,-12.5452301106633));
#64342=CARTESIAN_POINT('Ctrl Pts',(-20.9619064946779,26.5137452040934,-12.5511028044599));
#64343=CARTESIAN_POINT('Ctrl Pts',(-20.8771993318483,26.4352612995827,-12.5569754982565));
#64344=CARTESIAN_POINT('Ctrl Pts',(-20.8540079276428,26.4137737194026,-12.5585833435798));
#64345=CARTESIAN_POINT('Ctrl Pts',(-20.831085721933,26.3920158286571,-12.5601911889032));
#64346=CARTESIAN_POINT('Ctrl Pts',(-20.8084391801246,26.3699951698005,-12.5617990342266));
#64347=CARTESIAN_POINT('Ctrl Pts',(-20.7257277296633,26.2895696174335,-12.5676713311953));
#64348=CARTESIAN_POINT('Ctrl Pts',(-20.6464193968664,26.2053669851818,-12.573543628164));
#64349=CARTESIAN_POINT('Ctrl Pts',(-20.5708789761065,26.1177069550997,-12.5794159251327));
#64350=CARTESIAN_POINT('Ctrl Pts',(-20.4954364497325,26.0301605254548,-12.5852806120709));
#64351=CARTESIAN_POINT('Ctrl Pts',(-20.4237523923954,25.9391659183717,-12.5911452990091));
#64352=CARTESIAN_POINT('Ctrl Pts',(-20.3561560239427,25.8450807385911,-12.5970099859473));
#64353=CARTESIAN_POINT('Ctrl Pts',(-20.2886291741234,25.7510923195281,-12.6028686414221));
#64354=CARTESIAN_POINT('Ctrl Pts',(-20.2251818911019,25.6540199835902,-12.6087272968969));
#64355=CARTESIAN_POINT('Ctrl Pts',(-20.1661037843444,25.5542550905276,-12.6145859523717));
#64356=CARTESIAN_POINT('Ctrl Pts',(-20.1047180347016,25.4505932928701,-12.6206734520897));
#64357=CARTESIAN_POINT('Ctrl Pts',(-20.048050044221,25.3440246470571,-12.6267609518076));
#64358=CARTESIAN_POINT('Ctrl Pts',(-19.9963759310729,25.2350225775926,-12.6328484515255));
#64359=CARTESIAN_POINT('Ctrl Pts',(-19.9467019744684,25.1302396652499,-12.6387003216089));
#64360=CARTESIAN_POINT('Ctrl Pts',(-19.9016426799514,25.0232086165073,-12.6445521916922));
#64361=CARTESIAN_POINT('Ctrl Pts',(-19.8613965411944,24.9143751366508,-12.6504040617756));
#64362=CARTESIAN_POINT('Ctrl Pts',(-19.8211565302779,24.8055582276812,-12.6562550408586));
#64363=CARTESIAN_POINT('Ctrl Pts',(-19.785728361326,24.6949398208807,-12.6621060199416));
#64364=CARTESIAN_POINT('Ctrl Pts',(-19.7552619033032,24.58298440901,-12.6679569990245));
#64365=CARTESIAN_POINT('Ctrl Pts',(-19.7247927060526,24.4710189312705,-12.6738085041668));
#64366=CARTESIAN_POINT('Ctrl Pts',(-19.6992862151009,24.3577166083961,-12.6796600093091));
#64367=CARTESIAN_POINT('Ctrl Pts',(-19.6788418763863,24.2435551625623,-12.6855115144514));
#64368=CARTESIAN_POINT('Ctrl Pts',(-19.6583907485519,24.1293558061975,-12.6913649627512));
#64369=CARTESIAN_POINT('Ctrl Pts',(-19.64300518841,24.0142971662741,-12.6972184110509));
#64370=CARTESIAN_POINT('Ctrl Pts',(-19.6327330717947,23.8988644668155,-12.7030718593507));
#64371=CARTESIAN_POINT('Ctrl Pts',(-19.6224492735524,23.7833004953119,-12.7089319642922));
#64372=CARTESIAN_POINT('Ctrl Pts',(-19.6172905622549,23.6673620272137,-12.7147920692338));
#64373=CARTESIAN_POINT('Ctrl Pts',(-19.6172527413712,23.5515367900416,-12.7206521741753));
#64374=CARTESIAN_POINT('Ctrl Pts',(-19.6172148950175,23.4356335518215,-12.7265162255308));
#64375=CARTESIAN_POINT('Ctrl Pts',(-19.6223047878136,23.3198441083393,-12.7323802768862));
#64376=CARTESIAN_POINT('Ctrl Pts',(-19.6324662760574,23.2046518153413,-12.7382443282417));
#64377=CARTESIAN_POINT('Ctrl Pts',(-19.6426427403065,23.0892897518981,-12.7441170220382));
#64378=CARTESIAN_POINT('Ctrl Pts',(-19.6579056634082,22.9745270036465,-12.7499897158348));
#64379=CARTESIAN_POINT('Ctrl Pts',(-19.6781476765945,22.8608375687633,-12.7558624096314));
#64380=CARTESIAN_POINT('Ctrl Pts',(-19.6836896011975,22.8297113032836,-12.7574702549547));
#64381=CARTESIAN_POINT('Ctrl Pts',(-19.6896044558134,22.7986654046952,-12.7590781002781));
#64382=CARTESIAN_POINT('Ctrl Pts',(-19.6958893896751,22.7677093894686,-12.7606859456015));
#64383=CARTESIAN_POINT('Ctrl Pts',(-19.7188437109196,22.6546494379067,-12.7665582425702));
#64384=CARTESIAN_POINT('Ctrl Pts',(-19.74681528221,22.5424109145349,-12.7724305395389));
#64385=CARTESIAN_POINT('Ctrl Pts',(-19.7797323364932,22.4314735286818,-12.7783028365076));
#64386=CARTESIAN_POINT('Ctrl Pts',(-19.8126067328883,22.3206799088703,-12.7841675234458));
#64387=CARTESIAN_POINT('Ctrl Pts',(-19.8504137506637,22.2111844660361,-12.790032210384));
#64388=CARTESIAN_POINT('Ctrl Pts',(-19.8930304882355,22.1034574788828,-12.7958968973222));
#64389=CARTESIAN_POINT('Ctrl Pts',(-19.9356033971604,21.9958412821921,-12.801755552797));
#64390=CARTESIAN_POINT('Ctrl Pts',(-19.9829760358943,21.8899903056891,-12.8076142082718));
#64391=CARTESIAN_POINT('Ctrl Pts',(-20.0349756931068,21.7863597492125,-12.8134728637467));
#64392=CARTESIAN_POINT('Ctrl Pts',(-20.0890065027307,21.6786812919234,-12.8195603634646));
#64393=CARTESIAN_POINT('Ctrl Pts',(-20.1480330413069,21.573400689915,-12.8256478631825));
#64394=CARTESIAN_POINT('Ctrl Pts',(-20.2118062624334,21.4710061520512,-12.8317353629004));
#64395=CARTESIAN_POINT('Ctrl Pts',(-20.2731110052878,21.3725750127336,-12.8375872329838));
#64396=CARTESIAN_POINT('Ctrl Pts',(-20.3388015635028,21.2768110530268,-12.8434391030672));
#64397=CARTESIAN_POINT('Ctrl Pts',(-20.4086102519881,21.1841221915897,-12.8492909731506));
#64398=CARTESIAN_POINT('Ctrl Pts',(-20.4784083114659,21.0914474428744,-12.8551419522336));
#64399=CARTESIAN_POINT('Ctrl Pts',(-20.552323005865,21.0018471915897,-12.8609929313165));
#64400=CARTESIAN_POINT('Ctrl Pts',(-20.6300445601613,20.9156986030384,-12.8668439103995));
#64401=CARTESIAN_POINT('Ctrl Pts',(-20.7077731023733,20.8295422688999,-12.8726954155418));
#64402=CARTESIAN_POINT('Ctrl Pts',(-20.7893089079657,20.746838521368,-12.8785469206841));
#64403=CARTESIAN_POINT('Ctrl Pts',(-20.8743038160025,20.6679292550669,-12.8843984258264));
#64404=CARTESIAN_POINT('Ctrl Pts',(-20.959326948998,20.5889937847161,-12.8902518741262));
#64405=CARTESIAN_POINT('Ctrl Pts',(-21.0478111657511,20.5138555822654,-12.896105322426));
#64406=CARTESIAN_POINT('Ctrl Pts',(-21.1393741180676,20.442817210612,-12.9019587707257));
#64407=CARTESIAN_POINT('Ctrl Pts',(-21.2310411973434,20.3716980529044,-12.9078188756673));
#64408=CARTESIAN_POINT('Ctrl Pts',(-21.3257936736492,20.3046882855481,-12.9136789806088));
#64409=CARTESIAN_POINT('Ctrl Pts',(-21.4232189452357,20.2420480153323,-12.9195390855504));
#64410=CARTESIAN_POINT('Ctrl Pts',(-21.5207098266449,20.179365560815,-12.9254031369058));
#64411=CARTESIAN_POINT('Ctrl Pts',(-21.6208767310226,20.1210586701587,-12.9312671882613));
#64412=CARTESIAN_POINT('Ctrl Pts',(-21.7232826550185,20.0673413829969,-12.9371312396167));
#64413=CARTESIAN_POINT('Ctrl Pts',(-21.8258395049041,20.0135449272769,-12.9430039334133));
#64414=CARTESIAN_POINT('Ctrl Pts',(-21.9306415875036,19.9643517499993,-12.9488766272098));
#64415=CARTESIAN_POINT('Ctrl Pts',(-22.0372320828273,19.9199277361269,-12.9547493210064));
#64416=CARTESIAN_POINT('Ctrl Pts',(-22.0664147774055,19.9077651842517,-12.9563571663297));
#64417=CARTESIAN_POINT('Ctrl Pts',(-22.0957314424514,19.8959598263653,-12.9579650116531));
#64418=CARTESIAN_POINT('Ctrl Pts',(-22.1251725306378,19.8845144081249,-12.9595728569764));
#64419=CARTESIAN_POINT('Ctrl Pts',(-22.2326995485701,19.8427125669505,-12.9654451539451));
#64420=CARTESIAN_POINT('Ctrl Pts',(-22.34224752153,19.8055758391798,-12.9713174509138));
#64421=CARTESIAN_POINT('Ctrl Pts',(-22.4533740688761,19.7733031492155,-12.9771897478825));
#64422=CARTESIAN_POINT('Ctrl Pts',(-22.5643566050423,19.7410722820945,-12.9830544348207));
#64423=CARTESIAN_POINT('Ctrl Pts',(-22.6769132541011,19.7136930317912,-12.9889191217589));
#64424=CARTESIAN_POINT('Ctrl Pts',(-22.7905819291723,19.691316204717,-12.9947838086971));
#64425=CARTESIAN_POINT('Ctrl Pts',(-22.9041337031271,19.6689623908086,-13.0006424641719));
#64426=CARTESIAN_POINT('Ctrl Pts',(-23.0187948251574,19.651600846464,-13.0065011196468));
#64427=CARTESIAN_POINT('Ctrl Pts',(-23.1340889702056,19.6393323215532,-13.0123597751216));
#64428=CARTESIAN_POINT('Ctrl Pts',(-23.2538866061091,19.6265845772535,-13.0184472748395));
#64429=CARTESIAN_POINT('Ctrl Pts',(-23.3743672894156,19.6193359659724,-13.0245347745574));
#64430=CARTESIAN_POINT('Ctrl Pts',(-23.4949856616789,19.6176408583811,-13.0306222742753));
#64431=CARTESIAN_POINT('Ctrl Pts',(-23.610935243094,19.6160113635373,-13.0364741443587));
#64432=CARTESIAN_POINT('Ctrl Pts',(-23.7270116006823,19.6195134523921,-13.0423260144421));
#64433=CARTESIAN_POINT('Ctrl Pts',(-23.8427268504927,19.6281424143156,-13.0481778845255));
#64434=CARTESIAN_POINT('Ctrl Pts',(-23.9584244816041,19.6367700624013,-13.0540288636084));
#64435=CARTESIAN_POINT('Ctrl Pts',(-24.073760702134,19.6505230007146,-13.0598798426914));
#64436=CARTESIAN_POINT('Ctrl Pts',(-24.1882507500522,19.6693444841656,-13.0657308217744));
#64437=CARTESIAN_POINT('Ctrl Pts',(-24.3027510917275,19.6881676598491,-13.0715823269167));
#64438=CARTESIAN_POINT('Ctrl Pts',(-24.4164047016209,19.7120602195202,-13.077433832059));
#64439=CARTESIAN_POINT('Ctrl Pts',(-24.528735742303,19.7409140580801,-13.0832853372013));
#64440=CARTESIAN_POINT('Ctrl Pts',(-24.6411040856784,19.7697774783717,-13.0891387855011));
#64441=CARTESIAN_POINT('Ctrl Pts',(-24.7521485863547,19.8036053507769,-13.0949922338008));
#64442=CARTESIAN_POINT('Ctrl Pts',(-24.8614080176822,19.8422395474176,-13.1008456821006));
#64443=CARTESIAN_POINT('Ctrl Pts',(-24.9707917007082,19.8809176795292,-13.1067057870421));
#64444=CARTESIAN_POINT('Ctrl Pts',(-25.0783858725773,19.924412907624,-13.1125658919837));
#64445=CARTESIAN_POINT('Ctrl Pts',(-25.1837486723467,19.9725187016736,-13.1184259969252));
#64446=CARTESIAN_POINT('Ctrl Pts',(-25.2891824273672,20.0206568919648,-13.1242900482807));
#64447=CARTESIAN_POINT('Ctrl Pts',(-25.3923814509564,20.0734116430386,-13.1301540996361));
#64448=CARTESIAN_POINT('Ctrl Pts',(-25.4929294491425,20.1305309941398,-13.1360181509915));
#64449=CARTESIAN_POINT('Ctrl Pts',(-25.5936256350067,20.1877345277624,-13.1418908447881));
#64450=CARTESIAN_POINT('Ctrl Pts',(-25.6916626489464,20.2493152804833,-13.1477635385847));
#64451=CARTESIAN_POINT('Ctrl Pts',(-25.7866539985887,20.3149785898352,-13.1536362323813));
#64452=CARTESIAN_POINT('Ctrl Pts',(-25.8126610411095,20.3329561055227,-13.1552440777046));
#64453=CARTESIAN_POINT('Ctrl Pts',(-25.8384399870517,20.3512394113058,-13.1568519230279));
#64454=CARTESIAN_POINT('Ctrl Pts',(-25.8639833657127,20.3698219590025,-13.1584597683513));
#64455=CARTESIAN_POINT('Ctrl Pts',(-25.9564731617271,20.4371073431602,-13.1642816013966));
#64456=CARTESIAN_POINT('Ctrl Pts',(-26.0461934153803,20.5085530008612,-13.1701034344419));
#64457=CARTESIAN_POINT('Ctrl Pts',(-26.1327414871855,20.5839012721895,-13.1759252674872));
#64458=CARTESIAN_POINT('Ctrl Pts',(-26.2191770473706,20.6591515915252,-13.1817395322084));
#64459=CARTESIAN_POINT('Ctrl Pts',(-26.3024483088353,20.7382941652882,-13.1875537969295));
#64460=CARTESIAN_POINT('Ctrl Pts',(-26.3821821172197,20.8210284986355,-13.1933680616506));
#64461=CARTESIAN_POINT('Ctrl Pts',(-26.461834529825,20.9036783731357,-13.1991763909145));
#64462=CARTESIAN_POINT('Ctrl Pts',(-26.5379563791802,20.9899124152296,-13.2049847201784));
#64463=CARTESIAN_POINT('Ctrl Pts',(-26.6102086912381,21.0793908800291,-13.2107930494423));
#64464=CARTESIAN_POINT('Ctrl Pts',(-26.6824087585795,21.1688046441028,-13.2165971787781));
#64465=CARTESIAN_POINT('Ctrl Pts',(-26.7507445891201,21.2614578389486,-13.2224013081139));
#64466=CARTESIAN_POINT('Ctrl Pts',(-26.8149156222302,21.3569755529949,-13.2282054374497));
#64467=CARTESIAN_POINT('Ctrl Pts',(-26.8790624624768,21.4524572562917,-13.234007378594));
#64468=CARTESIAN_POINT('Ctrl Pts',(-26.9390473910909,21.550800983448,-13.2398093197383));
#64469=CARTESIAN_POINT('Ctrl Pts',(-26.9946119623445,21.6516011386021,-13.2456112608827));
#64470=CARTESIAN_POINT('Ctrl Pts',(-27.0501696158159,21.7523887441495,-13.251412479686));
#64471=CARTESIAN_POINT('Ctrl Pts',(-27.1013078028738,21.8556318007637,-13.2572136984894));
#64472=CARTESIAN_POINT('Ctrl Pts',(-27.1478134295246,21.9608990196015,-13.2630149172928));
#64473=CARTESIAN_POINT('Ctrl Pts',(-27.1943250094988,22.0661797140085,-13.2688168787274));
#64474=CARTESIAN_POINT('Ctrl Pts',(-27.2362026809513,22.1734847000118,-13.274618840162));
#64475=CARTESIAN_POINT('Ctrl Pts',(-27.2732813313051,22.2823623324783,-13.2804208015967));
#64476=CARTESIAN_POINT('Ctrl Pts',(-27.31039617053,22.391346229832,-13.2862284257626));
#64477=CARTESIAN_POINT('Ctrl Pts',(-27.3427024994715,22.5019054393114,-13.2920360499285));
#64478=CARTESIAN_POINT('Ctrl Pts',(-27.3700849821292,22.6135727301591,-13.2978436740944));
#64479=CARTESIAN_POINT('Ctrl Pts',(-27.39748145559,22.7252970762822,-13.3036542656073));
#64480=CARTESIAN_POINT('Ctrl Pts',(-27.4199489912256,22.8381302181769,-13.3094648571202));
#64481=CARTESIAN_POINT('Ctrl Pts',(-27.437423677328,22.9515961322864,-13.3152754486331));
#64482=CARTESIAN_POINT('Ctrl Pts',(-27.4549253614099,23.0652373485672,-13.3210950173733));
#64483=CARTESIAN_POINT('Ctrl Pts',(-27.4674187440957,23.1795128710186,-13.3269145861136));
#64484=CARTESIAN_POINT('Ctrl Pts',(-27.4748919119119,23.2939426894247,-13.3327341548538));
#64485=CARTESIAN_POINT('Ctrl Pts',(-27.4805003377686,23.379819411065,-13.3371015958909));
#64486=CARTESIAN_POINT('Ctrl Pts',(-27.4832823996245,23.4657829595106,-13.341469036928));
#64487=CARTESIAN_POINT('Ctrl Pts',(-27.4832522897918,23.5516319533889,-13.3458364779651));
#64488=CARTESIAN_POINT('',(-27.4832508627744,23.5466293120366,-14.5958364779651));
#64489=CARTESIAN_POINT('Ctrl Pts',(-27.4891703390607,23.5516340290274,-13.3458364779651));
#64490=CARTESIAN_POINT('Ctrl Pts',(-27.4895124260083,23.6271647418024,-13.3496732118855));
#64491=CARTESIAN_POINT('Ctrl Pts',(-27.4875288934805,23.702677131584,-13.3535099458058));
#64492=CARTESIAN_POINT('Ctrl Pts',(-27.4077260247039,25.0804599026187,-13.4236423168511));
#64493=CARTESIAN_POINT('Ctrl Pts',(-25.8343164901973,27.6028816370497,-13.5562335911011));
#64494=CARTESIAN_POINT('Ctrl Pts',(-21.3753410672612,27.6624916971593,-13.7551205024758));
#64495=CARTESIAN_POINT('Ctrl Pts',(-18.914924878056,23.9433026245908,-13.9540074138508));
#64496=CARTESIAN_POINT('Ctrl Pts',(-20.7139817915703,19.8629338418023,-14.1528943252257));
#64497=CARTESIAN_POINT('Ctrl Pts',(-25.1193310391543,19.1708983019559,-14.3517812366005));
#64498=CARTESIAN_POINT('Ctrl Pts',(-27.3193395389436,21.6446333378869,-14.4994286208471));
#64499=CARTESIAN_POINT('Ctrl Pts',(-27.4862333707757,23.2491136935675,-14.5807803679686));
#64500=CARTESIAN_POINT('Ctrl Pts',(-27.4834731626111,23.546629107246,-14.5958364779651));
#64501=CARTESIAN_POINT('',(-27.4832525228614,23.5505161199331,-15.8458364779913));
#64502=CARTESIAN_POINT('Ctrl Pts',(-27.4832508627744,23.5466293120366,-14.5958364779651));
#64503=CARTESIAN_POINT('Ctrl Pts',(-27.483356110635,23.6608756728268,-14.6016184276768));
#64504=CARTESIAN_POINT('Ctrl Pts',(-27.4784791878884,23.7752670552024,-14.6074003773886));
#64505=CARTESIAN_POINT('Ctrl Pts',(-27.4686089715413,23.8893274648705,-14.6131823271003));
#64506=CARTESIAN_POINT('Ctrl Pts',(-27.4587462040328,24.0033017956168,-14.6189599132998));
#64507=CARTESIAN_POINT('Ctrl Pts',(-27.4438976715182,24.116945228161,-14.6247374994993));
#64508=CARTESIAN_POINT('Ctrl Pts',(-27.4241043175623,24.2297827673178,-14.6305150856988));
#64509=CARTESIAN_POINT('Ctrl Pts',(-27.404318832571,24.342575447245,-14.6362903749848));
#64510=CARTESIAN_POINT('Ctrl Pts',(-27.3795925050751,24.4545624520454,-14.6420656642708));
#64511=CARTESIAN_POINT('Ctrl Pts',(-27.3500179328278,24.5652756330804,-14.6478409535568));
#64512=CARTESIAN_POINT('Ctrl Pts',(-27.3204475107449,24.6759732778671,-14.6536154324033));
#64513=CARTESIAN_POINT('Ctrl Pts',(-27.2860303059289,24.7853970433522,-14.6593899112499));
#64514=CARTESIAN_POINT('Ctrl Pts',(-27.24690945734,24.8930915295174,-14.6651643900964));
#64515=CARTESIAN_POINT('Ctrl Pts',(-27.2077840352198,25.0007986060054,-14.6709395440245));
#64516=CARTESIAN_POINT('Ctrl Pts',(-27.1639540226431,25.10677560197,-14.6767146979525));
#64517=CARTESIAN_POINT('Ctrl Pts',(-27.1156112958667,25.2105855954915,-14.6824898518805));
#64518=CARTESIAN_POINT('Ctrl Pts',(-27.0672201349842,25.3144995952322,-14.6882707918789));
#64519=CARTESIAN_POINT('Ctrl Pts',(-27.014307410922,25.4162418706406,-14.6940517318773));
#64520=CARTESIAN_POINT('Ctrl Pts',(-26.9571117307415,25.515398683477,-14.6998326718757));
#64521=CARTESIAN_POINT('Ctrl Pts',(-26.8998870056989,25.6146058496958,-14.7056165475259));
#64522=CARTESIAN_POINT('Ctrl Pts',(-26.8383752234161,25.7112245812216,-14.7114004231762));
#64523=CARTESIAN_POINT('Ctrl Pts',(-26.7728581599204,25.8048704516365,-14.7171842988264));
#64524=CARTESIAN_POINT('Ctrl Pts',(-26.7072344285476,25.8986687862441,-14.7229775911645));
#64525=CARTESIAN_POINT('Ctrl Pts',(-26.6375926502515,25.9894842550802,-14.7287708835027));
#64526=CARTESIAN_POINT('Ctrl Pts',(-26.5642548892321,26.0769655721394,-14.7345641758408));
#64527=CARTESIAN_POINT('Ctrl Pts',(-26.5009979495314,26.1524219307907,-14.7395611370107));
#64528=CARTESIAN_POINT('Ctrl Pts',(-26.4349920199945,26.2253982103105,-14.7445580981805));
#64529=CARTESIAN_POINT('Ctrl Pts',(-26.3664643341204,26.2956924024391,-14.7495550593504));
#64530=CARTESIAN_POINT('Ctrl Pts',(-26.2859324051439,26.378300282973,-14.7554273563191));
#64531=CARTESIAN_POINT('Ctrl Pts',(-26.2016277789585,26.4575001878523,-14.7612996532878));
#64532=CARTESIAN_POINT('Ctrl Pts',(-26.1138706068156,26.5329277344125,-14.7671719502566));
#64533=CARTESIAN_POINT('Ctrl Pts',(-26.0262271609984,26.6082575328626,-14.7730366371948));
#64534=CARTESIAN_POINT('Ctrl Pts',(-25.935140377456,26.6798244278518,-14.778901324133));
#64535=CARTESIAN_POINT('Ctrl Pts',(-25.8409682843132,26.7472996600148,-14.7847660110712));
#64536=CARTESIAN_POINT('Ctrl Pts',(-25.7468930412728,26.8147054981256,-14.790624666546));
#64537=CARTESIAN_POINT('Ctrl Pts',(-25.6497391339966,26.8780278040554,-14.7964833220208));
#64538=CARTESIAN_POINT('Ctrl Pts',(-25.5498982946156,26.9369774722275,-14.8023419774956));
#64539=CARTESIAN_POINT('Ctrl Pts',(-25.4461575841099,26.9982297663606,-14.8084294772135));
#64540=CARTESIAN_POINT('Ctrl Pts',(-25.3395160992451,27.0547605643504,-14.8145169769314));
#64541=CARTESIAN_POINT('Ctrl Pts',(-25.230447619476,27.106294357516,-14.8206044766493));
#64542=CARTESIAN_POINT('Ctrl Pts',(-25.1256008673807,27.1558334255216,-14.8264563467327));
#64543=CARTESIAN_POINT('Ctrl Pts',(-25.0185119194588,27.2007549420843,-14.8323082168161));
#64544=CARTESIAN_POINT('Ctrl Pts',(-24.9096267360728,27.2408609872839,-14.8381600868995));
#64545=CARTESIAN_POINT('Ctrl Pts',(-24.8007581314459,27.2809609259735,-14.8440110659825));
#64546=CARTESIAN_POINT('Ctrl Pts',(-24.6900942229466,27.3162467082954,-14.8498620450655));
#64547=CARTESIAN_POINT('Ctrl Pts',(-24.5780996958206,27.3465690631754,-14.8557130241484));
#64548=CARTESIAN_POINT('Ctrl Pts',(-24.4660950993092,27.3768941443267,-14.8615645292907));
#64549=CARTESIAN_POINT('Ctrl Pts',(-24.3527600453873,27.402254802873,-14.867416034433));
#64550=CARTESIAN_POINT('Ctrl Pts',(-24.2385723838139,27.4225522077495,-14.8732675395753));
#64551=CARTESIAN_POINT('Ctrl Pts',(-24.1243468030033,27.4428563529524,-14.8791209878751));
#64552=CARTESIAN_POINT('Ctrl Pts',(-24.0092684583377,27.4580938288264,-14.8849744361749));
#64553=CARTESIAN_POINT('Ctrl Pts',(-23.8938226350511,27.4682173840224,-14.8908278844746));
#64554=CARTESIAN_POINT('Ctrl Pts',(-23.7782455247951,27.478352451899,-14.8966879894162));
#64555=CARTESIAN_POINT('Ctrl Pts',(-23.6623005138431,27.4833619551266,-14.9025480943577));
#64556=CARTESIAN_POINT('Ctrl Pts',(-23.5464753239116,27.4832507179004,-14.9084081992993));
#64557=CARTESIAN_POINT('Ctrl Pts',(-23.4305721329638,27.4831394057629,-14.9142722506547));
#64558=CARTESIAN_POINT('Ctrl Pts',(-23.3147893356614,27.4779005051668,-14.9201363020102));
#64559=CARTESIAN_POINT('Ctrl Pts',(-23.199610215098,27.4675907818089,-14.9260003533656));
#64560=CARTESIAN_POINT('Ctrl Pts',(-23.0842613435028,27.4572658639769,-14.9318730471622));
#64561=CARTESIAN_POINT('Ctrl Pts',(-22.9695183324802,27.4418552627762,-14.9377457409587));
#64562=CARTESIAN_POINT('Ctrl Pts',(-22.8558550416392,27.421466956885,-14.9436184347553));
#64563=CARTESIAN_POINT('Ctrl Pts',(-22.824735933962,27.4158849797868,-14.9452262800786));
#64564=CARTESIAN_POINT('Ctrl Pts',(-22.7936976730415,27.4099301764103,-14.9468341254019));
#64565=CARTESIAN_POINT('Ctrl Pts',(-22.7627497716716,27.4036054097676,-14.9484419707252));
#64566=CARTESIAN_POINT('Ctrl Pts',(-22.6497194541605,27.3805056081604,-14.9543142676939));
#64567=CARTESIAN_POINT('Ctrl Pts',(-22.5375170209701,27.3523896177763,-14.9601865646626));
#64568=CARTESIAN_POINT('Ctrl Pts',(-22.4266220886732,27.3193298229575,-14.9660588616314));
#64569=CARTESIAN_POINT('Ctrl Pts',(-22.3158708674017,27.2863128710072,-14.9719235485695));
#64570=CARTESIAN_POINT('Ctrl Pts',(-22.2064241699327,27.2483649724142,-14.9777882355077));
#64571=CARTESIAN_POINT('Ctrl Pts',(-22.0987521164159,27.2056096338727,-14.9836529224459));
#64572=CARTESIAN_POINT('Ctrl Pts',(-21.9911907968657,27.1628982665204,-14.9895115779208));
#64573=CARTESIAN_POINT('Ctrl Pts',(-21.8854008729206,27.1153894450349,-14.9953702333956));
#64574=CARTESIAN_POINT('Ctrl Pts',(-21.7818373217765,27.0632564664104,-15.0012288888704));
#64575=CARTESIAN_POINT('Ctrl Pts',(-21.6742284871069,27.0090871277226,-15.0073163885883));
#64576=CARTESIAN_POINT('Ctrl Pts',(-21.5690239348475,26.9499251500729,-15.0134038883062));
#64577=CARTESIAN_POINT('Ctrl Pts',(-21.4667115529542,26.8860202079437,-15.0194913880241));
#64578=CARTESIAN_POINT('Ctrl Pts',(-21.3683593895854,26.8245888426284,-15.0253432581075));
#64579=CARTESIAN_POINT('Ctrl Pts',(-21.2726800478223,26.7587750980372,-15.0311951281909));
#64580=CARTESIAN_POINT('Ctrl Pts',(-21.1800811014959,26.6888471839983,-15.0370469982743));
#64581=CARTESIAN_POINT('Ctrl Pts',(-21.0874962542013,26.6189299171203,-15.0428979773573));
#64582=CARTESIAN_POINT('Ctrl Pts',(-20.9979911995804,26.5448999753691,-15.0487489564403));
#64583=CARTESIAN_POINT('Ctrl Pts',(-20.9119427039676,26.4670676188948,-15.0545999355232));
#64584=CARTESIAN_POINT('Ctrl Pts',(-20.8258864717669,26.3892282645427,-15.0604514406655));
#64585=CARTESIAN_POINT('Ctrl Pts',(-20.7432877229659,26.3075860931737,-15.0663029458078));
#64586=CARTESIAN_POINT('Ctrl Pts',(-20.6644879038494,26.2224897054271,-15.0721544509501));
#64587=CARTESIAN_POINT('Ctrl Pts',(-20.5856619170283,26.1373650590225,-15.0780078992499));
#64588=CARTESIAN_POINT('Ctrl Pts',(-20.5106376491086,26.0487842185151,-15.0838613475496));
#64589=CARTESIAN_POINT('Ctrl Pts',(-20.4397171706846,25.9571299211573,-15.0897147958494));
#64590=CARTESIAN_POINT('Ctrl Pts',(-20.3687160402766,25.8653713929611,-15.0955749007909));
#64591=CARTESIAN_POINT('Ctrl Pts',(-20.3018282674831,25.7705327587558,-15.1014350057325));
#64592=CARTESIAN_POINT('Ctrl Pts',(-20.2393134278915,25.6730269546865,-15.107295110674));
#64593=CARTESIAN_POINT('Ctrl Pts',(-20.176756488468,25.5754554865605,-15.1131591620295));
#64594=CARTESIAN_POINT('Ctrl Pts',(-20.1185785531158,25.4752136286926,-15.1190232133849));
#64595=CARTESIAN_POINT('Ctrl Pts',(-20.0649930989017,25.3727386595237,-15.1248872647404));
#64596=CARTESIAN_POINT('Ctrl Pts',(-20.0113286704249,25.2701126627063,-15.130759958537));
#64597=CARTESIAN_POINT('Ctrl Pts',(-19.9622704060186,25.1652473590959,-15.1366326523335));
#64598=CARTESIAN_POINT('Ctrl Pts',(-19.9179836026164,25.0585997817849,-15.1425053461301));
#64599=CARTESIAN_POINT('Ctrl Pts',(-19.9058586166724,25.0294014591127,-15.1441131914535));
#64600=CARTESIAN_POINT('Ctrl Pts',(-19.894090996831,25.0000696257647,-15.1457210367768));
#64601=CARTESIAN_POINT('Ctrl Pts',(-19.8826834764605,24.9706138325934,-15.1473288821002));
#64602=CARTESIAN_POINT('Ctrl Pts',(-19.8410200488168,24.8630331079819,-15.1532011790689));
#64603=CARTESIAN_POINT('Ctrl Pts',(-19.8040243315258,24.7534374336547,-15.1590734760376));
#64604=CARTESIAN_POINT('Ctrl Pts',(-19.771894679516,24.642269445887,-15.1649457730063));
#64605=CARTESIAN_POINT('Ctrl Pts',(-19.7398066649834,24.5312455230025,-15.1708104599445));
#64606=CARTESIAN_POINT('Ctrl Pts',(-19.7125722890121,24.4186537321826,-15.1766751468827));
#64607=CARTESIAN_POINT('Ctrl Pts',(-19.6903417632184,24.3049563540011,-15.1825398338209));
#64608=CARTESIAN_POINT('Ctrl Pts',(-19.6681341001289,24.1913759064559,-15.1883984892958));
#64609=CARTESIAN_POINT('Ctrl Pts',(-19.6509201301139,24.0766925364166,-15.1942571447706));
#64610=CARTESIAN_POINT('Ctrl Pts',(-19.6387999899668,23.9613826982038,-15.2001158002454));
#64611=CARTESIAN_POINT('Ctrl Pts',(-19.6262064264702,23.8415687561467,-15.2062032999633));
#64612=CARTESIAN_POINT('Ctrl Pts',(-19.6191128704675,23.721078844209,-15.2122907996812));
#64613=CARTESIAN_POINT('Ctrl Pts',(-19.6175729907506,23.6004583903563,-15.2183782993991));
#64614=CARTESIAN_POINT('Ctrl Pts',(-19.6160927153561,23.484506807924,-15.2242301694825));
#64615=CARTESIAN_POINT('Ctrl Pts',(-19.6197441825618,23.368435053373,-15.2300820395659));
#64616=CARTESIAN_POINT('Ctrl Pts',(-19.6285220538732,23.252731004188,-15.2359339096493));
#64617=CARTESIAN_POINT('Ctrl Pts',(-19.6372985886738,23.1370445719968,-15.2417848887322));
#64618=CARTESIAN_POINT('Ctrl Pts',(-19.6511999443506,23.0217261459378,-15.2476358678152));
#64619=CARTESIAN_POINT('Ctrl Pts',(-19.6701687520095,22.9072604146136,-15.2534868468982));
#64620=CARTESIAN_POINT('Ctrl Pts',(-19.6891392651468,22.7927843917183,-15.2593383520405));
#64621=CARTESIAN_POINT('Ctrl Pts',(-19.7131780683958,22.6791616238069,-15.2651898571828));
#64622=CARTESIAN_POINT('Ctrl Pts',(-19.7421764443815,22.5668678087919,-15.2710413623251));
#64623=CARTESIAN_POINT('Ctrl Pts',(-19.7711844500967,22.4545367034453,-15.2768948106249));
#64624=CARTESIAN_POINT('Ctrl Pts',(-19.805155200132,22.3435358285655,-15.2827482589247));
#64625=CARTESIAN_POINT('Ctrl Pts',(-19.8439299731772,22.2343262069221,-15.2886017072245));
#64626=CARTESIAN_POINT('Ctrl Pts',(-19.882748841559,22.1249923902251,-15.294461812166));
#64627=CARTESIAN_POINT('Ctrl Pts',(-19.9263824989732,22.0174542824313,-15.3003219171076));
#64628=CARTESIAN_POINT('Ctrl Pts',(-19.974623846922,21.9121534783296,-15.3061820220491));
#64629=CARTESIAN_POINT('Ctrl Pts',(-20.0228976823991,21.8067817607271,-15.3120460734045));
#64630=CARTESIAN_POINT('Ctrl Pts',(-20.0757851989103,21.7036507138604,-15.31791012476));
#64631=CARTESIAN_POINT('Ctrl Pts',(-20.1330339001709,21.6031763071025,-15.3237741761154));
#64632=CARTESIAN_POINT('Ctrl Pts',(-20.1903669745893,21.5025538211255,-15.329646869912));
#64633=CARTESIAN_POINT('Ctrl Pts',(-20.2520738423337,21.4045961380118,-15.3355195637085));
#64634=CARTESIAN_POINT('Ctrl Pts',(-20.3178593437951,21.3096893706065,-15.3413922575051));
#64635=CARTESIAN_POINT('Ctrl Pts',(-20.3358703136382,21.2837054852872,-15.3430001028284));
#64636=CARTESIAN_POINT('Ctrl Pts',(-20.3541867797811,21.2579500898859,-15.3446079481517));
#64637=CARTESIAN_POINT('Ctrl Pts',(-20.3728021844329,21.2324306466718,-15.3462157934751));
#64638=CARTESIAN_POINT('Ctrl Pts',(-20.4407908041852,21.1392265636325,-15.3520880904438));
#64639=CARTESIAN_POINT('Ctrl Pts',(-20.5129977302646,21.0488603378879,-15.3579603874125));
#64640=CARTESIAN_POINT('Ctrl Pts',(-20.5891577845937,20.9617381124386,-15.3638326843812));
#64641=CARTESIAN_POINT('Ctrl Pts',(-20.6652191415409,20.8747287904746,-15.3696973713194));
#64642=CARTESIAN_POINT('Ctrl Pts',(-20.7452231694908,20.790955416982,-15.3755620582576));
#64643=CARTESIAN_POINT('Ctrl Pts',(-20.8288621397872,20.7107942497615,-15.3814267451958));
#64644=CARTESIAN_POINT('Ctrl Pts',(-20.9124150926382,20.6307155232836,-15.3872854006706));
#64645=CARTESIAN_POINT('Ctrl Pts',(-20.9995952554929,20.5542418982105,-15.3931440561454));
#64646=CARTESIAN_POINT('Ctrl Pts',(-21.0900559075193,20.4817151650652,-15.3990027116203));
#64647=CARTESIAN_POINT('Ctrl Pts',(-21.1840500322909,20.4063554738422,-15.4050902113382));
#64648=CARTESIAN_POINT('Ctrl Pts',(-21.281585849077,20.3352576408274,-15.4111777110561));
#64649=CARTESIAN_POINT('Ctrl Pts',(-21.382233490436,20.2687616454137,-15.417265210774));
#64650=CARTESIAN_POINT('Ctrl Pts',(-21.4789853505966,20.2048395190466,-15.4231170808574));
#64651=CARTESIAN_POINT('Ctrl Pts',(-21.5786122380026,20.1451698557061,-15.4289689509408));
#64652=CARTESIAN_POINT('Ctrl Pts',(-21.6807008074574,20.0900118824903,-15.4348208210242));
#64653=CARTESIAN_POINT('Ctrl Pts',(-21.7827738329992,20.0348623075774,-15.4406718001072));
#64654=CARTESIAN_POINT('Ctrl Pts',(-21.8873074317477,19.9842232533686,-15.4465227791902));
#64655=CARTESIAN_POINT('Ctrl Pts',(-21.9938628167299,19.9383084491878,-15.4523737582732));
#64656=CARTESIAN_POINT('Ctrl Pts',(-22.1004277820665,19.8923895168242,-15.4582252634155));
#64657=CARTESIAN_POINT('Ctrl Pts',(-22.2090145153344,19.8511958424596,-15.4640767685578));
#64658=CARTESIAN_POINT('Ctrl Pts',(-22.3191640375484,19.81489309523,-15.4699282737001));
#64659=CARTESIAN_POINT('Ctrl Pts',(-22.4293501380207,19.7785782926485,-15.4757817219998));
#64660=CARTESIAN_POINT('Ctrl Pts',(-22.5410996669729,19.7471577760894,-15.4816351702996));
#64661=CARTESIAN_POINT('Ctrl Pts',(-22.6539389626171,19.7207472130025,-15.4874886185994));
#64662=CARTESIAN_POINT('Ctrl Pts',(-22.7669065810432,19.6943066153703,-15.4933487235409));
#64663=CARTESIAN_POINT('Ctrl Pts',(-22.8809660370256,19.6728874373227,-15.4992088284825));
#64664=CARTESIAN_POINT('Ctrl Pts',(-22.9956338639416,19.6565541441223,-15.505068933424));
#64665=CARTESIAN_POINT('Ctrl Pts',(-23.1103789124619,19.6402098514712,-15.5109329847794));
#64666=CARTESIAN_POINT('Ctrl Pts',(-23.2257327372844,19.628958303605,-15.5167970361349));
#64667=CARTESIAN_POINT('Ctrl Pts',(-23.3412088914505,19.6228119202433,-15.5226610874903));
#64668=CARTESIAN_POINT('Ctrl Pts',(-23.4568552344169,19.6166564783395,-15.5285337812869));
#64669=CARTESIAN_POINT('Ctrl Pts',(-23.5726238547347,19.615621221062,-15.5344064750835));
#64670=CARTESIAN_POINT('Ctrl Pts',(-23.6880303629076,19.6196665360409,-15.5402791688801));
#64671=CARTESIAN_POINT('Ctrl Pts',(-23.7196267343299,19.6207740756122,-15.5418870142034));
#64672=CARTESIAN_POINT('Ctrl Pts',(-23.7511960070516,19.6222621428333,-15.5434948595267));
#64673=CARTESIAN_POINT('Ctrl Pts',(-23.7827283581763,19.6241292541975,-15.54510270485));
#64674=CARTESIAN_POINT('Ctrl Pts',(-23.8978932482561,19.6309484626407,-15.5509750018187));
#64675=CARTESIAN_POINT('Ctrl Pts',(-24.0129507747762,19.6428505851457,-15.5568472987874));
#64676=CARTESIAN_POINT('Ctrl Pts',(-24.1274159028231,19.6598320604563,-15.5627195957561));
#64677=CARTESIAN_POINT('Ctrl Pts',(-24.2417326931544,19.6767915291235,-15.5685842826942));
#64678=CARTESIAN_POINT('Ctrl Pts',(-24.3554582065618,19.6988172003868,-15.5744489696324));
#64679=CARTESIAN_POINT('Ctrl Pts',(-24.4681095506604,19.7258535602564,-15.5803136565706));
#64680=CARTESIAN_POINT('Ctrl Pts',(-24.5806450399034,19.7528621149224,-15.5861723120454));
#64681=CARTESIAN_POINT('Ctrl Pts',(-24.6921081576227,19.784871012363,-15.5920309675201));
#64682=CARTESIAN_POINT('Ctrl Pts',(-24.8020239324085,19.8217733027922,-15.5978896229949));
#64683=CARTESIAN_POINT('Ctrl Pts',(-24.9162331141709,19.860117029189,-15.6039771227128));
#64684=CARTESIAN_POINT('Ctrl Pts',(-25.0287711577931,19.9037441555355,-15.6100646224307));
#64685=CARTESIAN_POINT('Ctrl Pts',(-25.139119671332,19.9524768004153,-15.6161521221487));
#64686=CARTESIAN_POINT('Ctrl Pts',(-25.2451969107647,19.999323144542,-15.622003992232));
#64687=CARTESIAN_POINT('Ctrl Pts',(-25.3492505558114,20.0508869338687,-15.6278558623154));
#64688=CARTESIAN_POINT('Ctrl Pts',(-25.4508390837635,20.1069605373822,-15.6337077323988));
#64689=CARTESIAN_POINT('Ctrl Pts',(-25.5524121439386,20.1630256031797,-15.6395587114817));
#64690=CARTESIAN_POINT('Ctrl Pts',(-25.6515204714959,20.2235989181551,-15.6454096905647));
#64691=CARTESIAN_POINT('Ctrl Pts',(-25.7477470694091,20.2884268532262,-15.6512606696476));
#64692=CARTESIAN_POINT('Ctrl Pts',(-25.8439823190194,20.3532606169526,-15.6571121747899));
#64693=CARTESIAN_POINT('Ctrl Pts',(-25.9373349810695,20.4223495302275,-15.6629636799322));
#64694=CARTESIAN_POINT('Ctrl Pts',(-26.0274175777364,20.4953969975213,-15.6688151850745));
#64695=CARTESIAN_POINT('Ctrl Pts',(-26.1175300888725,20.5684687222888,-15.6746686333742));
#64696=CARTESIAN_POINT('Ctrl Pts',(-26.2043700544324,20.6455013547467,-15.680522081674));
#64697=CARTESIAN_POINT('Ctrl Pts',(-26.2875841271733,20.7261589184456,-15.6863755299737));
#64698=CARTESIAN_POINT('Ctrl Pts',(-26.3708928323846,20.8069082073089,-15.6922356349153));
#64699=CARTESIAN_POINT('Ctrl Pts',(-26.4505671175344,20.891290367586,-15.6980957398568));
#64700=CARTESIAN_POINT('Ctrl Pts',(-26.5262914127103,20.9789334969028,-15.7039558447983));
#64701=CARTESIAN_POINT('Ctrl Pts',(-26.6020667034598,21.0666356483821,-15.7098198961538));
#64702=CARTESIAN_POINT('Ctrl Pts',(-26.6738864519735,21.1576028180315,-15.7156839475092));
#64703=CARTESIAN_POINT('Ctrl Pts',(-26.74147726413,21.2514324632482,-15.7215479988647));
#64704=CARTESIAN_POINT('Ctrl Pts',(-26.8091676916509,21.3454003946313,-15.7274206926612));
#64705=CARTESIAN_POINT('Ctrl Pts',(-26.8726165180301,21.4422388768522,-15.7332933864577));
#64706=CARTESIAN_POINT('Ctrl Pts',(-26.9315952367616,21.5415189727353,-15.7391660802543));
#64707=CARTESIAN_POINT('Ctrl Pts',(-26.9477426233586,21.5687002022379,-15.7407739255778));
#64708=CARTESIAN_POINT('Ctrl Pts',(-26.9635552176627,21.5960643244755,-15.7423817709013));
#64709=CARTESIAN_POINT('Ctrl Pts',(-26.9790289580811,21.6236022733822,-15.7439896162248));
#64710=CARTESIAN_POINT('Ctrl Pts',(-27.0381448271853,21.728808237742,-15.7501322275853));
#64711=CARTESIAN_POINT('Ctrl Pts',(-27.0924942057525,21.8368783305784,-15.7562748389458));
#64712=CARTESIAN_POINT('Ctrl Pts',(-27.1418029470715,21.9473630739327,-15.7624174503064));
#64713=CARTESIAN_POINT('Ctrl Pts',(-27.1910255695739,22.0576548532181,-15.7685493334592));
#64714=CARTESIAN_POINT('Ctrl Pts',(-27.2352249427918,22.1703525581504,-15.7746812166119));
#64715=CARTESIAN_POINT('Ctrl Pts',(-27.2741721621672,22.2849811830192,-15.7808130997647));
#64716=CARTESIAN_POINT('Ctrl Pts',(-27.3130334201259,22.3993568080807,-15.7869314490793));
#64717=CARTESIAN_POINT('Ctrl Pts',(-27.3466655169619,22.5156545194472,-15.793049798394));
#64718=CARTESIAN_POINT('Ctrl Pts',(-27.3748874772214,22.6333792942988,-15.7991681477086));
#64719=CARTESIAN_POINT('Ctrl Pts',(-27.4030721722485,22.7509486213695,-15.8052784181475));
#64720=CARTESIAN_POINT('Ctrl Pts',(-27.4258608715318,22.8699409127405,-15.8113886885864));
#64721=CARTESIAN_POINT('Ctrl Pts',(-27.4431219424024,22.989844866532,-15.8174989590254));
#64722=CARTESIAN_POINT('Ctrl Pts',(-27.4603550692174,23.1095547070631,-15.8235993375093));
#64723=CARTESIAN_POINT('Ctrl Pts',(-27.4720783532156,23.2301729141833,-15.8296997159932));
#64724=CARTESIAN_POINT('Ctrl Pts',(-27.4782110546695,23.3511775664535,-15.8358000944771));
#64725=CARTESIAN_POINT('Ctrl Pts',(-27.481574241821,23.4175367875645,-15.8391455556397));
#64726=CARTESIAN_POINT('Ctrl Pts',(-27.4832569799326,23.4840120305005,-15.8424910168024));
#64727=CARTESIAN_POINT('Ctrl Pts',(-27.4832525228614,23.5505161194119,-15.8458364779651));
#64728=CARTESIAN_POINT('',(-27.4832509455688,23.5537847349664,-17.0958364779651));
#64729=CARTESIAN_POINT('Ctrl Pts',(-27.4832525228614,23.550516119933,-15.8458364779913));
#64730=CARTESIAN_POINT('Ctrl Pts',(-27.48324431477,23.6729890476372,-15.8519974288415));
#64731=CARTESIAN_POINT('Ctrl Pts',(-27.477511140326,23.7953393043865,-15.8581583796916));
#64732=CARTESIAN_POINT('Ctrl Pts',(-27.4661129484295,23.9170306616928,-15.8643193305417));
#64733=CARTESIAN_POINT('Ctrl Pts',(-27.4546966094255,24.0389157643033,-15.8704900902668));
#64734=CARTESIAN_POINT('Ctrl Pts',(-27.4375972878388,24.1601395321258,-15.8766608499917));
#64735=CARTESIAN_POINT('Ctrl Pts',(-27.4149262183359,24.2801746479363,-15.8828316097167));
#64736=CARTESIAN_POINT('Ctrl Pts',(-27.3921961074326,24.4005223666145,-15.8890184397156));
#64737=CARTESIAN_POINT('Ctrl Pts',(-27.3638653041277,24.5196749056777,-15.8952052697145));
#64738=CARTESIAN_POINT('Ctrl Pts',(-27.3300956338617,24.6371173452736,-15.9013920997134));
#64739=CARTESIAN_POINT('Ctrl Pts',(-27.2962769719856,24.754730165396,-15.9075879053037));
#64740=CARTESIAN_POINT('Ctrl Pts',(-27.2570038069768,24.870627609844,-15.913783710894));
#64741=CARTESIAN_POINT('Ctrl Pts',(-27.2124864225242,24.9843138723824,-15.9199795164842));
#64742=CARTESIAN_POINT('Ctrl Pts',(-27.167867799437,25.0982586730654,-15.9261894121857));
#64743=CARTESIAN_POINT('Ctrl Pts',(-27.117981258964,25.2099819266785,-15.9323993078872));
#64744=CARTESIAN_POINT('Ctrl Pts',(-27.0630839286443,25.3190104508572,-15.9386092035887));
#64745=CARTESIAN_POINT('Ctrl Pts',(-27.0505091229324,25.343984570739,-15.9400316449257));
#64746=CARTESIAN_POINT('Ctrl Pts',(-27.0376715887623,25.3688174196986,-15.9414540862627));
#64747=CARTESIAN_POINT('Ctrl Pts',(-27.0245747344379,25.3935035269528,-15.9428765275997));
#64748=CARTESIAN_POINT('Ctrl Pts',(-26.9705066924393,25.495415745776,-15.9487488245684));
#64749=CARTESIAN_POINT('Ctrl Pts',(-26.9118601866573,25.5951177131025,-15.9546211215371));
#64750=CARTESIAN_POINT('Ctrl Pts',(-26.8488400501931,25.6921697529713,-15.9604934185059));
#64751=CARTESIAN_POINT('Ctrl Pts',(-26.7859015828207,25.7890960211042,-15.9663581054441));
#64752=CARTESIAN_POINT('Ctrl Pts',(-26.7186009791917,25.8833788474608,-15.9722227923823));
#64753=CARTESIAN_POINT('Ctrl Pts',(-26.6471894347301,25.974602097787,-15.9780874793205));
#64754=CARTESIAN_POINT('Ctrl Pts',(-26.5758513325716,26.0657315307109,-15.9839461347954));
#64755=CARTESIAN_POINT('Ctrl Pts',(-26.5004109522646,26.1538073227681,-15.9898047902702));
#64756=CARTESIAN_POINT('Ctrl Pts',(-26.4211629797005,26.2384419222559,-15.995663445745));
#64757=CARTESIAN_POINT('Ctrl Pts',(-26.3388195115278,26.3263824237444,-16.0017509454629));
#64758=CARTESIAN_POINT('Ctrl Pts',(-26.2523651789415,26.410607038867,-16.0078384451808));
#64759=CARTESIAN_POINT('Ctrl Pts',(-26.1621772293995,26.4907182045966,-16.0139259448987));
#64760=CARTESIAN_POINT('Ctrl Pts',(-26.0754801964193,26.5677284971313,-16.0197778149821));
#64761=CARTESIAN_POINT('Ctrl Pts',(-25.9853335451773,26.6409375586416,-16.0256296850655));
#64762=CARTESIAN_POINT('Ctrl Pts',(-25.8921096324298,26.7100301061026,-16.031481555149));
#64763=CARTESIAN_POINT('Ctrl Pts',(-25.7988999138706,26.7791121335951,-16.0373325342319));
#64764=CARTESIAN_POINT('Ctrl Pts',(-25.7026141974369,26.8440786471947,-16.0431835133149));
#64765=CARTESIAN_POINT('Ctrl Pts',(-25.6036564831716,26.9046557889155,-16.0490344923979));
#64766=CARTESIAN_POINT('Ctrl Pts',(-25.5046898716556,26.9652383771043,-16.0548859975402));
#64767=CARTESIAN_POINT('Ctrl Pts',(-25.4030511373262,27.0214305930544,-16.0607375026825));
#64768=CARTESIAN_POINT('Ctrl Pts',(-25.2991710907017,27.0730032855738,-16.0665890078248));
#64769=CARTESIAN_POINT('Ctrl Pts',(-25.1952565477747,27.1245931042618,-16.0724424561246));
#64770=CARTESIAN_POINT('Ctrl Pts',(-25.0890995826438,27.1715601654458,-16.0782959044244));
#64771=CARTESIAN_POINT('Ctrl Pts',(-24.9811526385236,27.2137227286899,-16.0841493527242));
#64772=CARTESIAN_POINT('Ctrl Pts',(-24.873082935288,27.2559332399236,-16.0900094576658));
#64773=CARTESIAN_POINT('Ctrl Pts',(-24.7632195753594,27.293328197237,-16.0958695626073));
#64774=CARTESIAN_POINT('Ctrl Pts',(-24.6520319765194,27.325775151804,-16.1017296675489));
#64775=CARTESIAN_POINT('Ctrl Pts',(-24.5407694997907,27.3582439573641,-16.1075937189043));
#64776=CARTESIAN_POINT('Ctrl Pts',(-24.4281814090004,27.3857580272712,-16.1134577702598));
#64777=CARTESIAN_POINT('Ctrl Pts',(-24.3147474608509,27.4082360079799,-16.1193218216153));
#64778=CARTESIAN_POINT('Ctrl Pts',(-24.2011463337053,27.4307471167452,-16.1251945154119));
#64779=CARTESIAN_POINT('Ctrl Pts',(-24.0866972682982,27.4482072609428,-16.1310672092084));
#64780=CARTESIAN_POINT('Ctrl Pts',(-23.9718853715709,27.4605868841937,-16.136939903005));
#64781=CARTESIAN_POINT('Ctrl Pts',(-23.9404517948184,27.4639762179536,-16.1385477483282));
#64782=CARTESIAN_POINT('Ctrl Pts',(-23.9089910197629,27.46698503117,-16.1401555936514));
#64783=CARTESIAN_POINT('Ctrl Pts',(-23.8775129804176,27.4696133977923,-16.1417634389746));
#64784=CARTESIAN_POINT('Ctrl Pts',(-23.7625464520062,27.4792129215314,-16.1476357359433));
#64785=CARTESIAN_POINT('Ctrl Pts',(-23.6469645914935,27.4837657722378,-16.153508032912));
#64786=CARTESIAN_POINT('Ctrl Pts',(-23.5312480266169,27.4832066159401,-16.1593803298807));
#64787=CARTESIAN_POINT('Ctrl Pts',(-23.4156814212184,27.4826481842646,-16.1652450168189));
#64788=CARTESIAN_POINT('Ctrl Pts',(-23.2999808681678,27.4769909218239,-16.1711097037571));
#64789=CARTESIAN_POINT('Ctrl Pts',(-23.1846322499708,27.4662212253373,-16.1769743906953));
#64790=CARTESIAN_POINT('Ctrl Pts',(-23.0694022606066,27.4554626048093,-16.1828330461701));
#64791=CARTESIAN_POINT('Ctrl Pts',(-22.9545238952912,27.4396020465045,-16.1886917016449));
#64792=CARTESIAN_POINT('Ctrl Pts',(-22.8404824979914,27.4186779864829,-16.1945503571198));
#64793=CARTESIAN_POINT('Ctrl Pts',(-22.7219865432668,27.3969366142473,-16.2006378568377));
#64794=CARTESIAN_POINT('Ctrl Pts',(-22.6043947296004,27.3697281086989,-16.2067253565556));
#64795=CARTESIAN_POINT('Ctrl Pts',(-22.4882454516809,27.3371549547838,-16.2128128562735));
#64796=CARTESIAN_POINT('Ctrl Pts',(-22.3765919788,27.3058426141265,-16.2186647263569));
#64797=CARTESIAN_POINT('Ctrl Pts',(-22.2662718804477,27.2695733252326,-16.2245165964403));
#64798=CARTESIAN_POINT('Ctrl Pts',(-22.1577516841349,27.2284899342481,-16.2303684665237));
#64799=CARTESIAN_POINT('Ctrl Pts',(-22.0492480110087,27.1874127985835,-16.2362194456067));
#64800=CARTESIAN_POINT('Ctrl Pts',(-21.9425440815196,27.141523164569,-16.2420704246896));
#64801=CARTESIAN_POINT('Ctrl Pts',(-21.8380886761361,27.0910128923682,-16.2479214037726));
#64802=CARTESIAN_POINT('Ctrl Pts',(-21.7336238792065,27.0404980788079,-16.2537729089149));
#64803=CARTESIAN_POINT('Ctrl Pts',(-21.631408380444,26.9853619811752,-16.2596244140572));
#64804=CARTESIAN_POINT('Ctrl Pts',(-21.5318678399399,26.9258431816534,-16.2654759191995));
#64805=CARTESIAN_POINT('Ctrl Pts',(-21.4322942441892,26.866304617234,-16.2713293674993));
#64806=CARTESIAN_POINT('Ctrl Pts',(-21.3353977276241,26.802380668987,-16.2771828157991));
#64807=CARTESIAN_POINT('Ctrl Pts',(-21.2415757562606,26.73435374657,-16.2830362640988));
#64808=CARTESIAN_POINT('Ctrl Pts',(-21.1476470889426,26.6662494627704,-16.2888963690404));
#64809=CARTESIAN_POINT('Ctrl Pts',(-21.0568002804533,26.5940331344607,-16.2947564739819));
#64810=CARTESIAN_POINT('Ctrl Pts',(-20.9694005024232,26.5180280964915,-16.3006165789235));
#64811=CARTESIAN_POINT('Ctrl Pts',(-20.8819418661128,26.4419718738861,-16.3064806302789));
#64812=CARTESIAN_POINT('Ctrl Pts',(-20.7979351814419,26.3621221452627,-16.3123446816344));
#64813=CARTESIAN_POINT('Ctrl Pts',(-20.7177082213493,26.2788385629443,-16.3182087329898));
#64814=CARTESIAN_POINT('Ctrl Pts',(-20.6373630227325,26.1954322372505,-16.3240814267864));
#64815=CARTESIAN_POINT('Ctrl Pts',(-20.5608089387756,26.1085822663961,-16.329954120583));
#64816=CARTESIAN_POINT('Ctrl Pts',(-20.4883330566234,26.0186808025139,-16.3358268143796));
#64817=CARTESIAN_POINT('Ctrl Pts',(-20.4684903724638,25.9940672855712,-16.3374346597029));
#64818=CARTESIAN_POINT('Ctrl Pts',(-20.4489531247863,25.9692251987545,-16.3390425050262));
#64819=CARTESIAN_POINT('Ctrl Pts',(-20.4297266211311,25.9441629396887,-16.3406503503495));
#64820=CARTESIAN_POINT('Ctrl Pts',(-20.3595060983629,25.8526286199332,-16.3465226473182));
#64821=CARTESIAN_POINT('Ctrl Pts',(-20.2931988132048,25.7578486702388,-16.3523949442869));
#64822=CARTESIAN_POINT('Ctrl Pts',(-20.2311195318906,25.6601921350039,-16.3582672412556));
#64823=CARTESIAN_POINT('Ctrl Pts',(-20.1691207003948,25.562662154883,-16.3641319281938));
#64824=CARTESIAN_POINT('Ctrl Pts',(-20.1113391963867,25.4622633481716,-16.369996615132));
#64825=CARTESIAN_POINT('Ctrl Pts',(-20.0580491046271,25.3593971428242,-16.3758613020702));
#64826=CARTESIAN_POINT('Ctrl Pts',(-20.0048138183908,25.2566367289294,-16.381719957545));
#64827=CARTESIAN_POINT('Ctrl Pts',(-19.9560609457124,25.1514143285916,-16.3875786130198));
#64828=CARTESIAN_POINT('Ctrl Pts',(-19.9120204986791,25.0441590461531,-16.3934372684946));
#64829=CARTESIAN_POINT('Ctrl Pts',(-19.8662597929943,24.9327142779133,-16.3995247682125));
#64830=CARTESIAN_POINT('Ctrl Pts',(-19.8255874048656,24.8190749613919,-16.4056122679304));
#64831=CARTESIAN_POINT('Ctrl Pts',(-19.7902081371419,24.7037494545317,-16.4116997676483));
#64832=CARTESIAN_POINT('Ctrl Pts',(-19.7561982992842,24.592887866898,-16.4175516377317));
#64833=CARTESIAN_POINT('Ctrl Pts',(-19.7270795706054,24.4804686289651,-16.4234035078151));
#64834=CARTESIAN_POINT('Ctrl Pts',(-19.7029839501431,24.3669614525529,-16.4292553778985));
#64835=CARTESIAN_POINT('Ctrl Pts',(-19.6788919984582,24.2534715586404,-16.4351063569815));
#64836=CARTESIAN_POINT('Ctrl Pts',(-19.6598217201127,24.1388944598719,-16.4409573360644));
#64837=CARTESIAN_POINT('Ctrl Pts',(-19.6458542848002,24.0237114313374,-16.4468083151474));
#64838=CARTESIAN_POINT('Ctrl Pts',(-19.631885593681,23.9085180467403,-16.4526598202897));
#64839=CARTESIAN_POINT('Ctrl Pts',(-19.6230207074027,23.7927190344791,-16.458511325432));
#64840=CARTESIAN_POINT('Ctrl Pts',(-19.6192889900959,23.6768014733149,-16.4643628305743));
#64841=CARTESIAN_POINT('Ctrl Pts',(-19.6155560335671,23.560845418452,-16.470216278874));
#64842=CARTESIAN_POINT('Ctrl Pts',(-19.6169596488206,23.4447711493564,-16.4760697271738));
#64843=CARTESIAN_POINT('Ctrl Pts',(-19.6234770871048,23.3290657152479,-16.4819231754736));
#64844=CARTESIAN_POINT('Ctrl Pts',(-19.6300019371315,23.2132286989359,-16.4877832804151));
#64845=CARTESIAN_POINT('Ctrl Pts',(-19.6416521945437,23.097761767785,-16.4936433853566));
#64846=CARTESIAN_POINT('Ctrl Pts',(-19.6583532230536,22.9831469230088,-16.4995034902982));
#64847=CARTESIAN_POINT('Ctrl Pts',(-19.6750654986609,22.8684548923081,-16.5053675416536));
#64848=CARTESIAN_POINT('Ctrl Pts',(-19.6968352407293,22.7546164956185,-16.511231593009));
#64849=CARTESIAN_POINT('Ctrl Pts',(-19.7235370428939,22.6421019011402,-16.5170956443645));
#64850=CARTESIAN_POINT('Ctrl Pts',(-19.7502781981846,22.5294214826098,-16.522968338161));
#64851=CARTESIAN_POINT('Ctrl Pts',(-19.7819658081179,22.4180691562552,-16.5288410319576));
#64852=CARTESIAN_POINT('Ctrl Pts',(-19.8184251312967,22.3084984281605,-16.5347137257542));
#64853=CARTESIAN_POINT('Ctrl Pts',(-19.8284070840936,22.2784997957013,-16.5363215710776));
#64854=CARTESIAN_POINT('Ctrl Pts',(-19.8387464379272,22.2486345803725,-16.537929416401));
#64855=CARTESIAN_POINT('Ctrl Pts',(-19.8494389966857,22.218911786769,-16.5395372617244));
#64856=CARTESIAN_POINT('Ctrl Pts',(-19.8884911862661,22.1103559025435,-16.5454095586931));
#64857=CARTESIAN_POINT('Ctrl Pts',(-19.9323892495922,22.0033378902027,-16.5512818556618));
#64858=CARTESIAN_POINT('Ctrl Pts',(-19.9809928479131,21.8983220520024,-16.5571541526305));
#64859=CARTESIAN_POINT('Ctrl Pts',(-20.0295334598306,21.7934423059883,-16.5630188395687));
#64860=CARTESIAN_POINT('Ctrl Pts',(-20.0827673079848,21.6905599459587,-16.5688835265069));
#64861=CARTESIAN_POINT('Ctrl Pts',(-20.140504818735,21.5901225528485,-16.5747482134451));
#64862=CARTESIAN_POINT('Ctrl Pts',(-20.1981829500698,21.4897884533097,-16.58060686892));
#64863=CARTESIAN_POINT('Ctrl Pts',(-20.260355326458,21.3918946754607,-16.5864655243948));
#64864=CARTESIAN_POINT('Ctrl Pts',(-20.3267852665007,21.2968666814178,-16.5923241798696));
#64865=CARTESIAN_POINT('Ctrl Pts',(-20.3958100185121,21.1981268102282,-16.5984116795875));
#64866=CARTESIAN_POINT('Ctrl Pts',(-20.4694315321615,21.1024815795919,-16.6044991793054));
#64867=CARTESIAN_POINT('Ctrl Pts',(-20.5473328220045,21.0103780826009,-16.6105866790233));
#64868=CARTESIAN_POINT('Ctrl Pts',(-20.6222187766026,20.9218396475133,-16.6164385491067));
#64869=CARTESIAN_POINT('Ctrl Pts',(-20.7010590603922,20.8365742086219,-16.6222904191902));
#64870=CARTESIAN_POINT('Ctrl Pts',(-20.7835298480138,20.7549467180831,-16.6281422892736));
#64871=CARTESIAN_POINT('Ctrl Pts',(-20.865988078708,20.6733316560719,-16.6339932683565));
#64872=CARTESIAN_POINT('Ctrl Pts',(-20.9520754204128,20.5953537317816,-16.6398442474395));
#64873=CARTESIAN_POINT('Ctrl Pts',(-21.0414308439804,20.521341384226,-16.6456952265225));
#64874=CARTESIAN_POINT('Ctrl Pts',(-21.1307943014606,20.4473223822481,-16.6515467316648));
#64875=CARTESIAN_POINT('Ctrl Pts',(-21.2234261065381,20.3772699294892,-16.6573982368071));
#64876=CARTESIAN_POINT('Ctrl Pts',(-21.3189323442364,20.3114720172037,-16.6632497419494));
#64877=CARTESIAN_POINT('Ctrl Pts',(-21.4144702974771,20.2456522548639,-16.6691031902492));
#64878=CARTESIAN_POINT('Ctrl Pts',(-21.5128842411385,20.1840900767431,-16.674956638549));
#64879=CARTESIAN_POINT('Ctrl Pts',(-21.6137521158751,20.1270296146856,-16.6808100868488));
#64880=CARTESIAN_POINT('Ctrl Pts',(-21.7147346992884,20.0699042624923,-16.6866701917903));
#64881=CARTESIAN_POINT('Ctrl Pts',(-21.8181764238196,20.0172910482463,-16.6925302967319));
#64882=CARTESIAN_POINT('Ctrl Pts',(-21.9236314296828,19.969387721276,-16.6983904016734));
#64883=CARTESIAN_POINT('Ctrl Pts',(-22.0291574528923,19.9214521344132,-16.7042544530289));
#64884=CARTESIAN_POINT('Ctrl Pts',(-22.1366990745092,19.8782329043107,-16.7101185043843));
#64885=CARTESIAN_POINT('Ctrl Pts',(-22.2457929466814,19.8398786703336,-16.7159825557398));
#64886=CARTESIAN_POINT('Ctrl Pts',(-22.355047601444,19.8014679098718,-16.7218552495364));
#64887=CARTESIAN_POINT('Ctrl Pts',(-22.4658586784054,19.7679365748165,-16.727727943333));
#64888=CARTESIAN_POINT('Ctrl Pts',(-22.5777501801553,19.7393827915625,-16.7336006371295));
#64889=CARTESIAN_POINT('Ctrl Pts',(-22.6083842016166,19.7315652433544,-16.7352084824528));
#64890=CARTESIAN_POINT('Ctrl Pts',(-22.6390991674193,19.7241205002501,-16.736816327776));
#64891=CARTESIAN_POINT('Ctrl Pts',(-22.6698852336702,19.7170498993553,-16.7384241730993));
#64892=CARTESIAN_POINT('Ctrl Pts',(-22.7823244844542,19.6912261042422,-16.744296470068));
#64893=CARTESIAN_POINT('Ctrl Pts',(-22.8960892980096,19.6703105089653,-16.7501687670367));
#64894=CARTESIAN_POINT('Ctrl Pts',(-23.010713190014,19.6544360192312,-16.7560410640054));
#64895=CARTESIAN_POINT('Ctrl Pts',(-23.1251885385575,19.6385821015751,-16.7619057509436));
#64896=CARTESIAN_POINT('Ctrl Pts',(-23.240520345906,19.6277563541092,-16.7677704378818));
#64897=CARTESIAN_POINT('Ctrl Pts',(-23.3562295821199,19.6220412218181,-16.77363512482));
#64898=CARTESIAN_POINT('Ctrl Pts',(-23.4718198186278,19.6163319671828,-16.7794937802948));
#64899=CARTESIAN_POINT('Ctrl Pts',(-23.5877863015297,19.6157228936424,-16.7853524357696));
#64900=CARTESIAN_POINT('Ctrl Pts',(-23.703643146079,19.6202448574754,-16.7912110912444));
#64901=CARTESIAN_POINT('Ctrl Pts',(-23.8240254610219,19.6249434531986,-16.7972985909623));
#64902=CARTESIAN_POINT('Ctrl Pts',(-23.9442889474807,19.6351821660237,-16.8033860906802));
#64903=CARTESIAN_POINT('Ctrl Pts',(-24.0638861144647,19.6509359835475,-16.8094735903981));
#64904=CARTESIAN_POINT('Ctrl Pts',(-24.1788540185246,19.6660800160304,-16.8153254604815));
#64905=CARTESIAN_POINT('Ctrl Pts',(-24.2932057785333,19.6863200852048,-16.8211773305649));
#64906=CARTESIAN_POINT('Ctrl Pts',(-24.4064593127839,19.7115810234747,-16.8270292006483));
#64907=CARTESIAN_POINT('Ctrl Pts',(-24.5196956031539,19.7368381155371,-16.8328801797312));
#64908=CARTESIAN_POINT('Ctrl Pts',(-24.6318335968848,19.76711446671,-16.8387311588142));
#64909=CARTESIAN_POINT('Ctrl Pts',(-24.7424018211641,19.8022838723246,-16.8445821378972));
#64910=CARTESIAN_POINT('Ctrl Pts',(-24.8529799865907,19.8374564400073,-16.8504336430394));
#64911=CARTESIAN_POINT('Ctrl Pts',(-24.9619877080391,19.8775228113676,-16.8562851481817));
#64912=CARTESIAN_POINT('Ctrl Pts',(-25.0689697658909,19.9223072506082,-16.862136653324));
#64913=CARTESIAN_POINT('Ctrl Pts',(-25.1759873501553,19.9671065617863,-16.8679901016238));
#64914=CARTESIAN_POINT('Ctrl Pts',(-25.2809775521256,20.0166268967214,-16.8738435499235));
#64915=CARTESIAN_POINT('Ctrl Pts',(-25.3835068386168,20.0706451334164,-16.8796969982233));
#64916=CARTESIAN_POINT('Ctrl Pts',(-25.4861527231704,20.1247248005762,-16.8855571031648));
#64917=CARTESIAN_POINT('Ctrl Pts',(-25.5863317403879,20.1833123862622,-16.8914172081063));
#64918=CARTESIAN_POINT('Ctrl Pts',(-25.6836365143257,20.246139673051,-16.8972773130479));
#64919=CARTESIAN_POINT('Ctrl Pts',(-25.7810068169388,20.3090092700853,-16.9031413644033));
#64920=CARTESIAN_POINT('Ctrl Pts',(-25.8754986858637,20.3761240146474,-16.9090054157587));
#64921=CARTESIAN_POINT('Ctrl Pts',(-25.9667366091519,20.4471744302934,-16.9148694671142));
#64922=CARTESIAN_POINT('Ctrl Pts',(-26.0581089989263,20.518329560069,-16.9207421609107));
#64923=CARTESIAN_POINT('Ctrl Pts',(-26.1462175584178,20.5934316702402,-16.9266148547073));
#64924=CARTESIAN_POINT('Ctrl Pts',(-26.2307224354649,20.6721333376754,-16.9324875485039));
#64925=CARTESIAN_POINT('Ctrl Pts',(-26.2538584572078,20.6936805377023,-16.9340953938273));
#64926=CARTESIAN_POINT('Ctrl Pts',(-26.2767245856099,20.7154973545247,-16.9357032391507));
#64927=CARTESIAN_POINT('Ctrl Pts',(-26.2993143747,20.7375762290725,-16.9373110844741));
#64928=CARTESIAN_POINT('Ctrl Pts',(-26.3806377699755,20.8170603285002,-16.9430993386388));
#64929=CARTESIAN_POINT('Ctrl Pts',(-26.4586662175932,20.900226228552,-16.9488875928034));
#64930=CARTESIAN_POINT('Ctrl Pts',(-26.5330404097928,20.9867655560557,-16.954675846968));
#64931=CARTESIAN_POINT('Ctrl Pts',(-26.6086152118127,21.0747018730712,-16.9605575399262));
#64932=CARTESIAN_POINT('Ctrl Pts',(-26.6804163740703,21.1661212422807,-16.9664392328845));
#64933=CARTESIAN_POINT('Ctrl Pts',(-26.7481028389295,21.2606581544048,-16.9723209258427));
#64934=CARTESIAN_POINT('Ctrl Pts',(-26.8145478422971,21.3534611314478,-16.9780947405814));
#64935=CARTESIAN_POINT('Ctrl Pts',(-26.8770275175112,21.449267917509,-16.9838685553201));
#64936=CARTESIAN_POINT('Ctrl Pts',(-26.9352579987848,21.5476974169054,-16.9896423700588));
#64937=CARTESIAN_POINT('Ctrl Pts',(-26.9934512704089,21.646064019223,-16.9954124952931));
#64938=CARTESIAN_POINT('Ctrl Pts',(-27.0474005270886,21.7470496392113,-17.0011826205273));
#64939=CARTESIAN_POINT('Ctrl Pts',(-27.0968649291307,21.8502438545547,-17.0069527457615));
#64940=CARTESIAN_POINT('Ctrl Pts',(-27.1463105048046,21.9533987937273,-17.0127206748608));
#64941=CARTESIAN_POINT('Ctrl Pts',(-27.1912744352322,22.0587602733001,-17.01848860396));
#64942=CARTESIAN_POINT('Ctrl Pts',(-27.2315620264637,22.1658936895872,-17.0242565330593));
#64943=CARTESIAN_POINT('Ctrl Pts',(-27.2732260782565,22.2766874121324,-17.0302215284681));
#64944=CARTESIAN_POINT('Ctrl Pts',(-27.3098883142778,22.389375888942,-17.0361865238769));
#64945=CARTESIAN_POINT('Ctrl Pts',(-27.3413880726729,22.5034572747656,-17.0421515192857));
#64946=CARTESIAN_POINT('Ctrl Pts',(-27.3718584508006,22.6138105962031,-17.0479215846735));
#64947=CARTESIAN_POINT('Ctrl Pts',(-27.3974984315432,22.7254667676748,-17.0536916500612));
#64948=CARTESIAN_POINT('Ctrl Pts',(-27.418214072793,22.8379586902349,-17.0594617154489));
#64949=CARTESIAN_POINT('Ctrl Pts',(-27.4399794682782,22.9561510818624,-17.0655241758682));
#64950=CARTESIAN_POINT('Ctrl Pts',(-27.4563082570169,23.0752656277984,-17.0715866362876));
#64951=CARTESIAN_POINT('Ctrl Pts',(-27.4671529931717,23.1947531999408,-17.077649096707));
#64952=CARTESIAN_POINT('Ctrl Pts',(-27.4779977293266,23.3142407720832,-17.0837115571264));
#64953=CARTESIAN_POINT('Ctrl Pts',(-27.4833584329987,23.434100826989,-17.0897740175457));
#64954=CARTESIAN_POINT('Ctrl Pts',(-27.4832509455688,23.5537847349664,-17.0958364779651));
#64955=CARTESIAN_POINT('',(-27.488632695345,23.5483506220125,-18.3458364779651));
#64956=CARTESIAN_POINT('Ctrl Pts',(-27.4844422471639,23.5537858048675,-17.0958364779651));
#64957=CARTESIAN_POINT('Ctrl Pts',(-27.4869069244524,23.8194717478141,-17.1092903172598));
#64958=CARTESIAN_POINT('Ctrl Pts',(-27.3410589034169,25.3916708787352,-17.1890397936792));
#64959=CARTESIAN_POINT('Ctrl Pts',(-25.2246752877004,27.8904206466729,-17.3350849072242));
#64960=CARTESIAN_POINT('Ctrl Pts',(-20.8038927595901,27.3050173491329,-17.5339718185988));
#64961=CARTESIAN_POINT('Ctrl Pts',(-18.9067820091341,23.2693035359248,-17.7328587299738));
#64962=CARTESIAN_POINT('Ctrl Pts',(-21.2766269675343,19.4917580292833,-17.9317456413486));
#64963=CARTESIAN_POINT('Ctrl Pts',(-25.735741047741,19.443624866767,-18.1306325527235));
#64964=CARTESIAN_POINT('Ctrl Pts',(-27.4366548782404,22.0291801880755,-18.2686628315957));
#64965=CARTESIAN_POINT('Ctrl Pts',(-27.489269671134,23.441238523299,-18.3403974733429));
#64966=CARTESIAN_POINT('Ctrl Pts',(-27.488632695345,23.5483506220125,-18.3458364779651));
#64967=CARTESIAN_POINT('',(-27.4785646527166,23.5476444295195,-19.5958364779651));
#64968=CARTESIAN_POINT('Ctrl Pts',(-27.488632695345,23.5483506220125,-18.3458364779651));
#64969=CARTESIAN_POINT('Ctrl Pts',(-27.4815056189417,24.7468202098731,-18.4066931104679));
#64970=CARTESIAN_POINT('Ctrl Pts',(-26.2565009221018,27.2634742278718,-18.5338453800956));
#64971=CARTESIAN_POINT('Ctrl Pts',(-21.9699074538095,27.92555369469,-18.7272932868482));
#64972=CARTESIAN_POINT('Ctrl Pts',(-19.0149947432021,24.5857174630311,-18.9261801982231));
#64973=CARTESIAN_POINT('Ctrl Pts',(-20.2275994137689,20.2943767524232,-19.1250671095979));
#64974=CARTESIAN_POINT('Ctrl Pts',(-24.4934405851835,18.99490983022,-19.3239540209729));
#64975=CARTESIAN_POINT('Ctrl Pts',(-27.1753782638637,21.2723832772041,-19.4808771437619));
#64976=CARTESIAN_POINT('Ctrl Pts',(-27.4814874096158,23.0653136103336,-19.571504629426));
#64977=CARTESIAN_POINT('Ctrl Pts',(-27.4785646527166,23.5476444295195,-19.5958364779651));
#64978=CARTESIAN_POINT('',(-27.4825985574987,23.5531384248387,-20.8458365189298));
#64979=CARTESIAN_POINT('Ctrl Pts',(-27.4785646527166,23.5476444295195,-19.5958364779651));
#64980=CARTESIAN_POINT('Ctrl Pts',(-27.4735239361261,24.3794936205995,-19.637800266551));
#64981=CARTESIAN_POINT('Ctrl Pts',(-26.8074519009194,26.5328992923714,-19.7460596922617));
#64982=CARTESIAN_POINT('Ctrl Pts',(-23.263327982895,28.1933576495441,-19.9206147550975));
#64983=CARTESIAN_POINT('Ctrl Pts',(-19.4888354106611,25.8186532460935,-20.1195016664724));
#64984=CARTESIAN_POINT('Ctrl Pts',(-19.4464408212713,21.3594809147753,-20.3183885778472));
#64985=CARTESIAN_POINT('Ctrl Pts',(-23.1751012479069,18.9134419526009,-20.5172754892222));
#64986=CARTESIAN_POINT('Ctrl Pts',(-26.7759790602274,20.517721770008,-20.6930914559281));
#64987=CARTESIAN_POINT('Ctrl Pts',(-27.4733101236253,22.6965827824429,-20.8026117855091));
#64988=CARTESIAN_POINT('Ctrl Pts',(-27.4790977446331,23.553135043743,-20.8458364779651));
#64989=CARTESIAN_POINT('',(-27.4847362990805,23.5517471200916,-22.0958364779651));
#64990=CARTESIAN_POINT('Ctrl Pts',(-27.4832514724493,23.553139055426,-20.8458365265699));
#64991=CARTESIAN_POINT('Ctrl Pts',(-27.483153468716,23.6866728888471,-20.852568041962));
#64992=CARTESIAN_POINT('Ctrl Pts',(-27.4762508629319,23.81993123264,-20.8592995573541));
#64993=CARTESIAN_POINT('Ctrl Pts',(-27.4626513953443,23.9522775703537,-20.8660310727461));
#64994=CARTESIAN_POINT('Ctrl Pts',(-27.4489790669834,24.0853329693935,-20.8727986530367));
#64995=CARTESIAN_POINT('Ctrl Pts',(-27.4285380422173,24.2174664225096,-20.8795662333272));
#64996=CARTESIAN_POINT('Ctrl Pts',(-27.4014871218311,24.3480502076328,-20.8863338136177));
#64997=CARTESIAN_POINT('Ctrl Pts',(-27.3742636811132,24.4794668057473,-20.8931445549238));
#64998=CARTESIAN_POINT('Ctrl Pts',(-27.3403458578836,24.6093137684927,-20.8999552962299));
#64999=CARTESIAN_POINT('Ctrl Pts',(-27.2999437608413,24.7369726697458,-20.906766037536));
#65000=CARTESIAN_POINT('Ctrl Pts',(-27.2835646501324,24.7887259060794,-20.9095271290147));
#65001=CARTESIAN_POINT('Ctrl Pts',(-27.2661203833671,24.8401197870983,-20.9122882204933));
#65002=CARTESIAN_POINT('Ctrl Pts',(-27.2476271470571,24.8911141776778,-20.9150493119719));
#65003=CARTESIAN_POINT('Ctrl Pts',(-27.2082956810897,24.999569188147,-20.9209216089406));
#65004=CARTESIAN_POINT('Ctrl Pts',(-27.1641223156677,25.1064738593099,-20.9267939059093));
#65005=CARTESIAN_POINT('Ctrl Pts',(-27.115248584118,25.2113642516585,-20.9326662028781));
#65006=CARTESIAN_POINT('Ctrl Pts',(-27.0664381890429,25.3161187143889,-20.9385308898163));
#65007=CARTESIAN_POINT('Ctrl Pts',(-27.0129397142333,25.4188637181002,-20.9443955767545));
#65008=CARTESIAN_POINT('Ctrl Pts',(-26.9549438847051,25.5191521712728,-20.9502602636927));
#65009=CARTESIAN_POINT('Ctrl Pts',(-26.897007700257,25.6193374840494,-20.9561189191675));
#65010=CARTESIAN_POINT('Ctrl Pts',(-26.8345835666454,25.7170709157408,-20.9619775746424));
#65011=CARTESIAN_POINT('Ctrl Pts',(-26.7679092595578,25.8119276148205,-20.9678362301172));
#65012=CARTESIAN_POINT('Ctrl Pts',(-26.6986305953095,25.9104895001147,-20.9739237298351));
#65013=CARTESIAN_POINT('Ctrl Pts',(-26.6247631497663,26.0059449237659,-20.980011229553));
#65014=CARTESIAN_POINT('Ctrl Pts',(-26.5466250580701,26.0978476100337,-20.9860987292709));
#65015=CARTESIAN_POINT('Ctrl Pts',(-26.4715114675385,26.1861930072046,-20.9919505993543));
#65016=CARTESIAN_POINT('Ctrl Pts',(-26.39245198509,26.2712552412002,-20.9978024694377));
#65017=CARTESIAN_POINT('Ctrl Pts',(-26.3097713743408,26.3526701945486,-21.0036543395211));
#65018=CARTESIAN_POINT('Ctrl Pts',(-26.2271033524663,26.4340727517301,-21.0095053186041));
#65019=CARTESIAN_POINT('Ctrl Pts',(-26.1408155930216,26.5118288424783,-21.0153562976871));
#65020=CARTESIAN_POINT('Ctrl Pts',(-26.0512699693086,26.5856109580993,-21.0212072767701));
#65021=CARTESIAN_POINT('Ctrl Pts',(-25.9617162945825,26.6593997074424,-21.0270587819124));
#65022=CARTESIAN_POINT('Ctrl Pts',(-25.8689044923576,26.7292135084934,-21.0329102870547));
#65023=CARTESIAN_POINT('Ctrl Pts',(-25.7732292175498,26.7947653848268,-21.038761792197));
#65024=CARTESIAN_POINT('Ctrl Pts',(-25.6775221710659,26.8603390295113,-21.0446152404968));
#65025=CARTESIAN_POINT('Ctrl Pts',(-25.5789501020386,26.9216477017333,-21.0504686887966));
#65026=CARTESIAN_POINT('Ctrl Pts',(-25.477935696772,26.9784483567712,-21.0563221370963));
#65027=CARTESIAN_POINT('Ctrl Pts',(-25.3768064161918,27.035313606488,-21.0621822420379));
#65028=CARTESIAN_POINT('Ctrl Pts',(-25.2732296161714,27.0876604037614,-21.0680423469794));
#65029=CARTESIAN_POINT('Ctrl Pts',(-25.1676516639953,27.1352921474909,-21.073902451921));
#65030=CARTESIAN_POINT('Ctrl Pts',(-25.0620026116764,27.1829559682186,-21.0797665032764));
#65031=CARTESIAN_POINT('Ctrl Pts',(-24.9543501067855,27.2258982599754,-21.0856305546319));
#65032=CARTESIAN_POINT('Ctrl Pts',(-24.8451578782144,27.2639715764731,-21.0914946059873));
#65033=CARTESIAN_POINT('Ctrl Pts',(-24.7358047220951,27.3021010054391,-21.0973672997839));
#65034=CARTESIAN_POINT('Ctrl Pts',(-24.6249077078045,27.3353470191755,-21.1032399935805));
#65035=CARTESIAN_POINT('Ctrl Pts',(-24.5129430837383,27.3636127167548,-21.1091126873771));
#65036=CARTESIAN_POINT('Ctrl Pts',(-24.4822890426096,27.3713513919243,-21.1107205327004));
#65037=CARTESIAN_POINT('Ctrl Pts',(-24.4515550169493,27.3787170548869,-21.1123283780236));
#65038=CARTESIAN_POINT('Ctrl Pts',(-24.4207508540594,27.3857083938779,-21.1139362233469));
#65039=CARTESIAN_POINT('Ctrl Pts',(-24.3082455093324,27.4112427025393,-21.1198085203156));
#65040=CARTESIAN_POINT('Ctrl Pts',(-24.1944272391577,27.4318654158323,-21.1256808172843));
#65041=CARTESIAN_POINT('Ctrl Pts',(-24.0797628683909,27.4474448291478,-21.131553114253));
#65042=CARTESIAN_POINT('Ctrl Pts',(-23.9652470935423,27.4630040527808,-21.1374178011912));
#65043=CARTESIAN_POINT('Ctrl Pts',(-23.8498878044433,27.4735329184888,-21.1432824881294));
#65044=CARTESIAN_POINT('Ctrl Pts',(-23.7341642416473,27.4789502145074,-21.1491471750676));
#65045=CARTESIAN_POINT('Ctrl Pts',(-23.6185596932913,27.4843619391763,-21.1550058305424));
#65046=CARTESIAN_POINT('Ctrl Pts',(-23.5025920268501,27.4846725312448,-21.1608644860173));
#65047=CARTESIAN_POINT('Ctrl Pts',(-23.3867472048801,27.4798523851276,-21.1667231414921));
#65048=CARTESIAN_POINT('Ctrl Pts',(-23.2663773821291,27.4748439598574,-21.17281064121));
#65049=CARTESIAN_POINT('Ctrl Pts',(-23.1461406468572,27.4642957416819,-21.1788981409279));
#65050=CARTESIAN_POINT('Ctrl Pts',(-23.0265844238634,27.4482341520768,-21.1849856406458));
#65051=CARTESIAN_POINT('Ctrl Pts',(-22.9116558789694,27.4327942604864,-21.1908375107292));
#65052=CARTESIAN_POINT('Ctrl Pts',(-22.797356592481,27.4122599349417,-21.1966893808126));
#65053=CARTESIAN_POINT('Ctrl Pts',(-22.6841684510391,27.3867075835925,-21.202541250896));
#65054=CARTESIAN_POINT('Ctrl Pts',(-22.5709975435209,27.361159122821,-21.2083922299789));
#65055=CARTESIAN_POINT('Ctrl Pts',(-22.458937847786,27.330594246407,-21.2142432090619));
#65056=CARTESIAN_POINT('Ctrl Pts',(-22.3484605102543,27.2951403720979,-21.2200941881449));
#65057=CARTESIAN_POINT('Ctrl Pts',(-22.2379732397468,27.2596833101443,-21.2259456932872));
#65058=CARTESIAN_POINT('Ctrl Pts',(-22.1290690038953,27.2193365027983,-21.2317971984295));
#65059=CARTESIAN_POINT('Ctrl Pts',(-22.022202568494,27.1742768569387,-21.2376487035718));
#65060=CARTESIAN_POINT('Ctrl Pts',(-21.9153006450761,27.1292022477517,-21.2435021518715));
#65061=CARTESIAN_POINT('Ctrl Pts',(-21.8104382484081,27.0794118486078,-21.2493556001713));
#65062=CARTESIAN_POINT('Ctrl Pts',(-21.7080483359584,27.0251298966113,-21.2552090484711));
#65063=CARTESIAN_POINT('Ctrl Pts',(-21.6055419839445,26.9707862142483,-21.2610691534126));
#65064=CARTESIAN_POINT('Ctrl Pts',(-21.5055140937677,26.9119409776187,-21.2669292583541));
#65065=CARTESIAN_POINT('Ctrl Pts',(-21.4083713496726,26.8488634517789,-21.2727893632957));
#65066=CARTESIAN_POINT('Ctrl Pts',(-21.3111631860194,26.7857434471733,-21.2786534146511));
#65067=CARTESIAN_POINT('Ctrl Pts',(-21.2168443728608,26.7183857177359,-21.2845174660066));
#65068=CARTESIAN_POINT('Ctrl Pts',(-21.1257896243579,26.6471007053944,-21.290381517362));
#65069=CARTESIAN_POINT('Ctrl Pts',(-21.034600679332,26.5757106331746,-21.2962542111586));
#65070=CARTESIAN_POINT('Ctrl Pts',(-20.9466857126837,26.5003819942177,-21.3021269049551));
#65071=CARTESIAN_POINT('Ctrl Pts',(-20.8623836812363,26.4214630852305,-21.3079995987517));
#65072=CARTESIAN_POINT('Ctrl Pts',(-20.8393031952265,26.3998564081016,-21.3096074440751));
#65073=CARTESIAN_POINT('Ctrl Pts',(-20.8164932956146,26.3779808097333,-21.3112152893984));
#65074=CARTESIAN_POINT('Ctrl Pts',(-20.7939604088947,26.3558438657615,-21.3128231347218));
#65075=CARTESIAN_POINT('Ctrl Pts',(-20.7116640583318,26.2749936079077,-21.3186954316905));
#65076=CARTESIAN_POINT('Ctrl Pts',(-20.6327902234969,26.1903838383324,-21.3245677286592));
#65077=CARTESIAN_POINT('Ctrl Pts',(-20.5577020483122,26.1023361126942,-21.3304400256279));
#65078=CARTESIAN_POINT('Ctrl Pts',(-20.4827111814391,26.014402489916,-21.3363047125661));
#65079=CARTESIAN_POINT('Ctrl Pts',(-20.4114964838776,25.9230400827357,-21.3421693995043));
#65080=CARTESIAN_POINT('Ctrl Pts',(-20.344385330283,25.8286081858703,-21.3480340864425));
#65081=CARTESIAN_POINT('Ctrl Pts',(-20.2773431963087,25.7342734062994,-21.3538927419173));
#65082=CARTESIAN_POINT('Ctrl Pts',(-20.2143964500605,25.6368757509681,-21.3597513973922));
#65083=CARTESIAN_POINT('Ctrl Pts',(-20.1558326825771,25.5368080652547,-21.365610052867));
#65084=CARTESIAN_POINT('Ctrl Pts',(-20.0949813627536,25.4328316475989,-21.3716975525849));
#65085=CARTESIAN_POINT('Ctrl Pts',(-20.0388627030738,25.3259727057584,-21.3777850523028));
#65086=CARTESIAN_POINT('Ctrl Pts',(-19.9877503810177,25.2167060793292,-21.3838725520207));
#65087=CARTESIAN_POINT('Ctrl Pts',(-19.938616470185,25.1116688502621,-21.3897244221041));
#65088=CARTESIAN_POINT('Ctrl Pts',(-19.8941087329581,25.004407269329,-21.3955762921875));
#65089=CARTESIAN_POINT('Ctrl Pts',(-19.8544233660366,24.8953680576899,-21.4014281622709));
#65090=CARTESIAN_POINT('Ctrl Pts',(-19.8147440415731,24.7863454482623,-21.4072791413539));
#65091=CARTESIAN_POINT('Ctrl Pts',(-19.7798857688329,24.6755461346364,-21.4131301204369));
#65092=CARTESIAN_POINT('Ctrl Pts',(-19.7499960237405,24.5634353748944,-21.4189810995198));
#65093=CARTESIAN_POINT('Ctrl Pts',(-19.7201035912723,24.4513145353162,-21.4248326046621));
#65094=CARTESIAN_POINT('Ctrl Pts',(-19.6951806809851,24.337882414679,-21.4306841098044));
#65095=CARTESIAN_POINT('Ctrl Pts',(-19.6753242783446,24.2236172407433,-21.4365356149467));
#65096=CARTESIAN_POINT('Ctrl Pts',(-19.655461281825,24.1093141218307,-21.4423890632465));
#65097=CARTESIAN_POINT('Ctrl Pts',(-19.6406682091888,23.9941778066043,-21.4482425115463));
#65098=CARTESIAN_POINT('Ctrl Pts',(-19.6309904378639,23.8786937591073,-21.4540959598461));
#65099=CARTESIAN_POINT('Ctrl Pts',(-19.6213016608115,23.7630783811716,-21.4599560647876));
#65100=CARTESIAN_POINT('Ctrl Pts',(-19.6167398305841,23.6471148938481,-21.4658161697292));
#65101=CARTESIAN_POINT('Ctrl Pts',(-19.6172982400469,23.5312909965933,-21.4716762746707));
#65102=CARTESIAN_POINT('Ctrl Pts',(-19.6178570255636,23.4153890991928,-21.4775403260262));
#65103=CARTESIAN_POINT('Ctrl Pts',(-19.6235428965134,23.2996273909202,-21.4834043773816));
#65104=CARTESIAN_POINT('Ctrl Pts',(-19.6342972217834,23.1844889321087,-21.4892684287371));
#65105=CARTESIAN_POINT('Ctrl Pts',(-19.6450673967821,23.0691807821928,-21.4951411225337));
#65106=CARTESIAN_POINT('Ctrl Pts',(-19.6609208781658,22.9544981229286,-21.5010138163302));
#65107=CARTESIAN_POINT('Ctrl Pts',(-19.6817478586037,22.8409143935139,-21.5068865101268));
#65108=CARTESIAN_POINT('Ctrl Pts',(-19.6874499374547,22.8098170684245,-21.5084943554501));
#65109=CARTESIAN_POINT('Ctrl Pts',(-19.6935245276755,22.7788020288813,-21.5101022007734));
#65110=CARTESIAN_POINT('Ctrl Pts',(-19.6999687295489,22.7478787765541,-21.5117100460967));
#65111=CARTESIAN_POINT('Ctrl Pts',(-19.7235047417377,22.6349384841817,-21.5175823430654));
#65112=CARTESIAN_POINT('Ctrl Pts',(-19.7520537090575,22.5228454362526,-21.5234546400341));
#65113=CARTESIAN_POINT('Ctrl Pts',(-19.7855413960222,22.4120789663066,-21.5293269370028));
#65114=CARTESIAN_POINT('Ctrl Pts',(-19.8189856856041,22.3014560409088,-21.535191623941));
#65115=CARTESIAN_POINT('Ctrl Pts',(-19.8573558486285,22.1921566667845,-21.5410563108792));
#65116=CARTESIAN_POINT('Ctrl Pts',(-19.9005265643013,22.0846504837501,-21.5469209978174));
#65117=CARTESIAN_POINT('Ctrl Pts',(-19.9436528815955,21.9772548640951,-21.5527796532922));
#65118=CARTESIAN_POINT('Ctrl Pts',(-19.9915697783382,21.8716491486544,-21.558638308767));
#65119=CARTESIAN_POINT('Ctrl Pts',(-20.04410220227,21.7682876421752,-21.5644969642418));
#65120=CARTESIAN_POINT('Ctrl Pts',(-20.0986865889506,21.660888744213,-21.5705844639597));
#65121=CARTESIAN_POINT('Ctrl Pts',(-20.158254295031,21.5559133861147,-21.5766719636776));
#65122=CARTESIAN_POINT('Ctrl Pts',(-20.2225537642718,21.4538484882676,-21.5827594633955));
#65123=CARTESIAN_POINT('Ctrl Pts',(-20.2843643856869,21.3557342295484,-21.5886113334789));
#65124=CARTESIAN_POINT('Ctrl Pts',(-20.3505470345989,21.2603096918223,-21.5944632035623));
#65125=CARTESIAN_POINT('Ctrl Pts',(-20.4208319296343,21.1679814103893,-21.6003150736457));
#65126=CARTESIAN_POINT('Ctrl Pts',(-20.4911061231554,21.0756671867768,-21.6061660527286));
#65127=CARTESIAN_POINT('Ctrl Pts',(-20.5654810705637,20.9864486109287,-21.6120170318116));
#65128=CARTESIAN_POINT('Ctrl Pts',(-20.6436450594176,20.9007012485321,-21.6178680108945));
#65129=CARTESIAN_POINT('Ctrl Pts',(-20.7218160759664,20.8149461766223,-21.6237195160368));
#65130=CARTESIAN_POINT('Ctrl Pts',(-20.8037765326829,20.7326632441018,-21.6295710211791));
#65131=CARTESIAN_POINT('Ctrl Pts',(-20.8891765132842,20.654192548848,-21.6354225263214));
#65132=CARTESIAN_POINT('Ctrl Pts',(-20.9746048533599,20.5756957951846,-21.6412759746211));
#65133=CARTESIAN_POINT('Ctrl Pts',(-21.0634746842623,20.5010140756193,-21.6471294229209));
#65134=CARTESIAN_POINT('Ctrl Pts',(-21.1554021053699,20.4304479808394,-21.6529828712207));
#65135=CARTESIAN_POINT('Ctrl Pts',(-21.2474340679171,20.3598016370865,-21.6588429761622));
#65136=CARTESIAN_POINT('Ctrl Pts',(-21.3425302328383,20.2932805118373,-21.6647030811037));
#65137=CARTESIAN_POINT('Ctrl Pts',(-21.4402766649077,20.2311425844977,-21.6705631860452));
#65138=CARTESIAN_POINT('Ctrl Pts',(-21.5380889230812,20.1689628111533,-21.6764272374007));
#65139=CARTESIAN_POINT('Ctrl Pts',(-21.6385546448185,20.1111723189739,-21.6822912887561));
#65140=CARTESIAN_POINT('Ctrl Pts',(-21.7412357307542,20.057982895209,-21.6881553401115));
#65141=CARTESIAN_POINT('Ctrl Pts',(-21.8440681481136,20.0047150808509,-21.6940280339081));
#65142=CARTESIAN_POINT('Ctrl Pts',(-21.9491220722908,19.9560620416572,-21.6999007277046));
#65143=CARTESIAN_POINT('Ctrl Pts',(-22.055939835428,19.912187308835,-21.7057734215012));
#65144=CARTESIAN_POINT('Ctrl Pts',(-22.085184752134,19.9001751409221,-21.7073812668246));
#65145=CARTESIAN_POINT('Ctrl Pts',(-22.1145617988165,19.8885208519009,-21.7089891121481));
#65146=CARTESIAN_POINT('Ctrl Pts',(-22.1440614141416,19.8772271382459,-21.7105969574715));
#65147=CARTESIAN_POINT('Ctrl Pts',(-22.2518021894051,19.8359793642871,-21.7164692544402));
#65148=CARTESIAN_POINT('Ctrl Pts',(-22.3615398784659,19.7994070451275,-21.7223415514089));
#65149=CARTESIAN_POINT('Ctrl Pts',(-22.472831082547,19.7677068253058,-21.7282138483776));
#65150=CARTESIAN_POINT('Ctrl Pts',(-22.5839780620662,19.7360476864513,-21.7340785353158));
#65151=CARTESIAN_POINT('Ctrl Pts',(-22.6966741591104,19.7092482031442,-21.739943222254));
#65152=CARTESIAN_POINT('Ctrl Pts',(-22.8104565166202,19.687456801128,-21.7458079091922));
#65153=CARTESIAN_POINT('Ctrl Pts',(-22.9241218560982,19.6656878102045,-21.751666564667));
#65154=CARTESIAN_POINT('Ctrl Pts',(-23.0388708304082,19.648916733256,-21.7575252201418));
#65155=CARTESIAN_POINT('Ctrl Pts',(-23.1542266021768,19.6372418668544,-21.7633838756166));
#65156=CARTESIAN_POINT('Ctrl Pts',(-23.274088271995,19.6251109698881,-21.7694713753345));
#65157=CARTESIAN_POINT('Ctrl Pts',(-23.3946046724564,19.6184826491818,-21.7755588750524));
#65158=CARTESIAN_POINT('Ctrl Pts',(-23.5152301724579,19.6174084673619,-21.7816463747703));
#65159=CARTESIAN_POINT('Ctrl Pts',(-23.6311866057169,19.616375864036,-21.7874982448537));
#65160=CARTESIAN_POINT('Ctrl Pts',(-23.747243397781,19.6204754290202,-21.7933501149371));
#65161=CARTESIAN_POINT('Ctrl Pts',(-23.8629126954122,19.6296999402826,-21.7992019850205));
#65162=CARTESIAN_POINT('Ctrl Pts',(-23.9785643813411,19.6389230470294,-21.8050529641035));
#65163=CARTESIAN_POINT('Ctrl Pts',(-24.0938282781855,19.6532695156755,-21.8109039431864));
#65164=CARTESIAN_POINT('Ctrl Pts',(-24.2082199224427,19.672680106489,-21.8167549222694));
#65165=CARTESIAN_POINT('Ctrl Pts',(-24.3226218516095,19.6920924425014,-21.8226064274117));
#65166=CARTESIAN_POINT('Ctrl Pts',(-24.4361509647081,19.7165697366414,-21.828457932554));
#65167=CARTESIAN_POINT('Ctrl Pts',(-24.548331987103,19.7460014357897,-21.8343094376963));
#65168=CARTESIAN_POINT('Ctrl Pts',(-24.6605502623735,19.7754429085646,-21.840162885996));
#65169=CARTESIAN_POINT('Ctrl Pts',(-24.7714191571347,19.809841952975,-21.8460163342958));
#65170=CARTESIAN_POINT('Ctrl Pts',(-24.8804782648373,19.8490380689963,-21.8518697825955));
#65171=CARTESIAN_POINT('Ctrl Pts',(-24.989661396427,19.8882787595128,-21.8577298875371));
#65172=CARTESIAN_POINT('Ctrl Pts',(-25.0970302437597,19.9323272703802,-21.8635899924786));
#65173=CARTESIAN_POINT('Ctrl Pts',(-25.2021440148948,19.9809747997533,-21.8694500974201));
#65174=CARTESIAN_POINT('Ctrl Pts',(-25.3073285735761,20.0296550901927,-21.8753141487756));
#65175=CARTESIAN_POINT('Ctrl Pts',(-25.4102546659133,20.0829403765934,-21.881178200131));
#65176=CARTESIAN_POINT('Ctrl Pts',(-25.5105073004607,20.1405765585953,-21.8870422514865));
#65177=CARTESIAN_POINT('Ctrl Pts',(-25.610907687379,20.1982976848241,-21.892914945283));
#65178=CARTESIAN_POINT('Ctrl Pts',(-25.7086264051352,20.2603822836222,-21.8987876390796));
#65179=CARTESIAN_POINT('Ctrl Pts',(-25.8032784833016,20.3265337068921,-21.9046603328761));
#65180=CARTESIAN_POINT('Ctrl Pts',(-25.8291926389689,20.344644860006,-21.9062681781995));
#65181=CARTESIAN_POINT('Ctrl Pts',(-25.8548771269737,20.3630606249987,-21.9078760235229));
#65182=CARTESIAN_POINT('Ctrl Pts',(-25.8803245104205,20.3817744153181,-21.9094838688464));
#65183=CARTESIAN_POINT('Ctrl Pts',(-25.9724125688686,20.4494951937751,-21.9153022805674));
#65184=CARTESIAN_POINT('Ctrl Pts',(-26.0617139492967,20.521357777344,-21.9211206922885));
#65185=CARTESIAN_POINT('Ctrl Pts',(-26.1478276033948,20.5971029000501,-21.9269391040095));
#65186=CARTESIAN_POINT('Ctrl Pts',(-26.2338292961867,20.672749542173,-21.9327499508794));
#65187=CARTESIAN_POINT('Ctrl Pts',(-26.3166511878312,20.7522684131351,-21.9385607977493));
#65188=CARTESIAN_POINT('Ctrl Pts',(-26.3959219135356,20.8353575485963,-21.9443716446192));
#65189=CARTESIAN_POINT('Ctrl Pts',(-26.4751117596737,20.9183619085847,-21.9501765627081));
#65190=CARTESIAN_POINT('Ctrl Pts',(-26.550757354672,21.0049289869369,-21.955981480797));
#65191=CARTESIAN_POINT('Ctrl Pts',(-26.6225217010584,21.0947177323126,-21.9617863988858));
#65192=CARTESIAN_POINT('Ctrl Pts',(-26.6942341937376,21.1844416003563,-21.9675871226005));
#65193=CARTESIAN_POINT('Ctrl Pts',(-26.762070752269,21.2773821779639,-21.9733878463151));
#65194=CARTESIAN_POINT('Ctrl Pts',(-26.8257329654358,21.3731634365545,-21.9791885700298));
#65195=CARTESIAN_POINT('Ctrl Pts',(-26.8893712767439,21.4689087342511,-21.9849871158736));
#65196=CARTESIAN_POINT('Ctrl Pts',(-26.9488381241163,21.567492242681,-21.9907856617174));
#65197=CARTESIAN_POINT('Ctrl Pts',(-27.0038773656675,21.6685074623071,-21.9965842075612));
#65198=CARTESIAN_POINT('Ctrl Pts',(-27.0589098750446,21.7695103261661,-22.0023820441507));
#65199=CARTESIAN_POINT('Ctrl Pts',(-27.1095156537141,21.8729439395001,-22.0081798807402));
#65200=CARTESIAN_POINT('Ctrl Pts',(-27.1554840438975,21.9783763459162,-22.0139777173297));
#65201=CARTESIAN_POINT('Ctrl Pts',(-27.2014584478216,22.0838225453569,-22.0197763124118));
#65202=CARTESIAN_POINT('Ctrl Pts',(-27.2427940897842,22.1912676706322,-22.0255749074939));
#65203=CARTESIAN_POINT('Ctrl Pts',(-27.2793284004151,22.3002596655853,-22.031373502576));
#65204=CARTESIAN_POINT('Ctrl Pts',(-27.3158981278116,22.4093573185858,-22.0371777188804));
#65205=CARTESIAN_POINT('Ctrl Pts',(-27.3476570957907,22.5200044350151,-22.0429819351848));
#65206=CARTESIAN_POINT('Ctrl Pts',(-27.3744925979449,22.6317336610754,-22.0487861514892));
#65207=CARTESIAN_POINT('Ctrl Pts',(-27.401341916976,22.7435204135032,-22.0545933562282));
#65208=CARTESIAN_POINT('Ctrl Pts',(-27.423262642645,22.8563899711206,-22.0604005609671));
#65209=CARTESIAN_POINT('Ctrl Pts',(-27.4401935372969,22.9698664766146,-22.0662077657061));
#65210=CARTESIAN_POINT('Ctrl Pts',(-27.4571501620944,23.0835154341303,-22.072023795745));
#65211=CARTESIAN_POINT('Ctrl Pts',(-27.4691017686041,23.1977727624032,-22.0778398257839));
#65212=CARTESIAN_POINT('Ctrl Pts',(-27.4760391345818,23.3121589606166,-22.0836558558228));
#65213=CARTESIAN_POINT('Ctrl Pts',(-27.4808821536785,23.3920126895583,-22.0877160632036));
#65214=CARTESIAN_POINT('Ctrl Pts',(-27.483282568071,23.4719291877988,-22.0917762705843));
#65215=CARTESIAN_POINT('Ctrl Pts',(-27.4832522479274,23.5517465563465,-22.0958364779651));
#65216=CARTESIAN_POINT('',(-27.4832508741802,23.5466417143109,-23.3458364779651));
#65217=CARTESIAN_POINT('Ctrl Pts',(-27.4890683231693,23.5517487656932,-22.0958364779651));
#65218=CARTESIAN_POINT('Ctrl Pts',(-27.4894675906155,23.6340053585404,-22.1000145787172));
#65219=CARTESIAN_POINT('Ctrl Pts',(-27.4871150503414,23.7162386824283,-22.1041926794693));
#65220=CARTESIAN_POINT('Ctrl Pts',(-27.3997979165351,25.1002966205361,-22.1746664173463));
#65221=CARTESIAN_POINT('Ctrl Pts',(-25.8134246394771,27.6145855449525,-22.3072576915961));
#65222=CARTESIAN_POINT('Ctrl Pts',(-21.3542014421887,27.6512414910049,-22.5061446029711));
#65223=CARTESIAN_POINT('Ctrl Pts',(-18.9129630017294,23.9194362899765,-22.7050315143459));
#65224=CARTESIAN_POINT('Ctrl Pts',(-20.7330004619926,19.8483825167044,-22.903918425721));
#65225=CARTESIAN_POINT('Ctrl Pts',(-25.1418537107282,19.1790334203933,-23.1028053370958));
#65226=CARTESIAN_POINT('Ctrl Pts',(-27.3240420942646,21.6583151087892,-23.2501113545105));
#65227=CARTESIAN_POINT('Ctrl Pts',(-27.4863816571791,23.2559105440861,-23.3311217348003));
#65228=CARTESIAN_POINT('Ctrl Pts',(-27.4836796968938,23.5466413206162,-23.3458364779651));
#65229=CARTESIAN_POINT('',(-27.4832525287817,23.5504038905352,-24.5958364779952));
#65230=CARTESIAN_POINT('Ctrl Pts',(-27.4832508741802,23.5466417143109,-23.3458364779651));
#65231=CARTESIAN_POINT('Ctrl Pts',(-27.4833557182763,23.6608406926443,-23.3516171098966));
#65232=CARTESIAN_POINT('Ctrl Pts',(-27.4784825236897,23.7751880197479,-23.3573977418282));
#65233=CARTESIAN_POINT('Ctrl Pts',(-27.4686193057639,23.889208021201,-23.3631783737597));
#65234=CARTESIAN_POINT('Ctrl Pts',(-27.4587638157106,24.003138687505,-23.3689544765419));
#65235=CARTESIAN_POINT('Ctrl Pts',(-27.4439261121891,24.1167421157918,-23.3747305793241));
#65236=CARTESIAN_POINT('Ctrl Pts',(-27.4241462761573,24.2295435272252,-23.3805066821063));
#65237=CARTESIAN_POINT('Ctrl Pts',(-27.4043746756592,24.3422979726569,-23.38628037995));
#65238=CARTESIAN_POINT('Ctrl Pts',(-27.379665103976,24.454250646175,-23.3920540777937));
#65239=CARTESIAN_POINT('Ctrl Pts',(-27.3501093088941,24.5649335026246,-23.3978277756374));
#65240=CARTESIAN_POINT('Ctrl Pts',(-27.3205582084652,24.6755987781697,-23.4036005563849));
#65241=CARTESIAN_POINT('Ctrl Pts',(-27.2861625243139,24.7849942264451,-23.4093733371324));
#65242=CARTESIAN_POINT('Ctrl Pts',(-27.2470645714314,24.8926644442061,-23.4151461178799));
#65243=CARTESIAN_POINT('Ctrl Pts',(-27.2079627601056,25.0003452875728,-23.4209194683233));
#65244=CARTESIAN_POINT('Ctrl Pts',(-27.164157904009,25.1063001623625,-23.4266928187668));
#65245=CARTESIAN_POINT('Ctrl Pts',(-27.1158410934982,25.210092044398,-23.4324661692103));
#65246=CARTESIAN_POINT('Ctrl Pts',(-27.0674764450961,25.3139866895237,-23.4382452357784));
#65247=CARTESIAN_POINT('Ctrl Pts',(-27.0145911004505,25.415713678327,-23.4440243023465));
#65248=CARTESIAN_POINT('Ctrl Pts',(-26.9574229325611,25.5148590723166,-23.4498033689146));
#65249=CARTESIAN_POINT('Ctrl Pts',(-26.9002266367599,25.6140532478746,-23.455585278902));
#65250=CARTESIAN_POINT('Ctrl Pts',(-26.838743551296,25.7106629410969,-23.4613671888895));
#65251=CARTESIAN_POINT('Ctrl Pts',(-26.7732547789132,25.8043034438124,-23.4671490988769));
#65252=CARTESIAN_POINT('Ctrl Pts',(-26.7076582898858,25.8980979674447,-23.4729405190127));
#65253=CARTESIAN_POINT('Ctrl Pts',(-26.6380432119247,25.9889132072198,-23.4787319391486));
#65254=CARTESIAN_POINT('Ctrl Pts',(-26.5647310345513,26.0763974910765,-23.4845233592844));
#65255=CARTESIAN_POINT('Ctrl Pts',(-26.4969822112343,26.1572429590788,-23.4898752928048));
#65256=CARTESIAN_POINT('Ctrl Pts',(-26.426076723758,26.2352440384564,-23.4952272263252));
#65257=CARTESIAN_POINT('Ctrl Pts',(-26.3522944087462,26.3101529500511,-23.5005791598455));
#65258=CARTESIAN_POINT('Ctrl Pts',(-26.2713383088362,26.3923451844673,-23.5064514568142));
#65259=CARTESIAN_POINT('Ctrl Pts',(-26.1866271048295,26.4711100677901,-23.512323753783));
#65260=CARTESIAN_POINT('Ctrl Pts',(-26.0984828194568,26.5460848702154,-23.5181960507517));
#65261=CARTESIAN_POINT('Ctrl Pts',(-26.0104527620777,26.6209625112511,-23.5240607376899));
#65262=CARTESIAN_POINT('Ctrl Pts',(-25.9189987827724,26.692059573523,-23.529925424628));
#65263=CARTESIAN_POINT('Ctrl Pts',(-25.824480597266,26.7590491450316,-23.5357901115662));
#65264=CARTESIAN_POINT('Ctrl Pts',(-25.7300596177961,26.8259698219597,-23.5416487670411));
#65265=CARTESIAN_POINT('Ctrl Pts',(-25.6325810355479,26.8887911728701,-23.5475074225159));
#65266=CARTESIAN_POINT('Ctrl Pts',(-25.5324380656816,26.9472261125234,-23.5533660779907));
#65267=CARTESIAN_POINT('Ctrl Pts',(-25.4283834232077,27.0079435723882,-23.5594535777086));
#65268=CARTESIAN_POINT('Ctrl Pts',(-25.3214523495019,27.0639246664437,-23.5655410774265));
#65269=CARTESIAN_POINT('Ctrl Pts',(-25.2121200359687,27.1148963285183,-23.5716285771445));
#65270=CARTESIAN_POINT('Ctrl Pts',(-25.1070196623568,27.1638950239134,-23.5774804472279));
#65271=CARTESIAN_POINT('Ctrl Pts',(-24.9997008922467,27.2082646869657,-23.5833323173113));
#65272=CARTESIAN_POINT('Ctrl Pts',(-24.8906106989184,27.2478096960333,-23.5891841873947));
#65273=CARTESIAN_POINT('Ctrl Pts',(-24.7815371155639,27.2873486840137,-23.5950351664776));
#65274=CARTESIAN_POINT('Ctrl Pts',(-24.6706930338013,27.3220643377828,-23.6008861455606));
#65275=CARTESIAN_POINT('Ctrl Pts',(-24.5585439011175,27.3518097802894,-23.6067371246436));
#65276=CARTESIAN_POINT('Ctrl Pts',(-24.4463846851479,27.3815578971973,-23.6125886297859));
#65277=CARTESIAN_POINT('Ctrl Pts',(-24.3329205845939,27.4063348085226,-23.6184401349282));
#65278=CARTESIAN_POINT('Ctrl Pts',(-24.2186299516329,27.426044144322,-23.6242916400704));
#65279=CARTESIAN_POINT('Ctrl Pts',(-24.1043013652403,27.4457600251628,-23.6301450883702));
#65280=CARTESIAN_POINT('Ctrl Pts',(-23.9891461078219,27.4604049140596,-23.63599853667));
#65281=CARTESIAN_POINT('Ctrl Pts',(-23.8736497014162,27.4699340583767,-23.6418519849698));
#65282=CARTESIAN_POINT('Ctrl Pts',(-23.7580219505167,27.4794740394,-23.6477120899113));
#65283=CARTESIAN_POINT('Ctrl Pts',(-23.6420526884998,27.4838866298542,-23.6535721948528));
#65284=CARTESIAN_POINT('Ctrl Pts',(-23.5262296057866,27.4831791644997,-23.6594322997944));
#65285=CARTESIAN_POINT('Ctrl Pts',(-23.4103285234763,27.4824712227116,-23.6652963511499));
#65286=CARTESIAN_POINT('Ctrl Pts',(-23.2945742283383,27.4766363801485,-23.6711604025053));
#65287=CARTESIAN_POINT('Ctrl Pts',(-23.179449704852,27.4657338895359,-23.6770244538608));
#65288=CARTESIAN_POINT('Ctrl Pts',(-23.0641555107995,27.4548153308285,-23.6828971476573));
#65289=CARTESIAN_POINT('Ctrl Pts',(-22.9494933487008,27.4388142749035,-23.6887698414539));
#65290=CARTESIAN_POINT('Ctrl Pts',(-22.8359365160484,27.41784113828,-23.6946425352505));
#65291=CARTESIAN_POINT('Ctrl Pts',(-22.8048465548419,27.4120990443101,-23.6962503805738));
#65292=CARTESIAN_POINT('Ctrl Pts',(-22.7738393585066,27.405984545174,-23.6978582258971));
#65293=CARTESIAN_POINT('Ctrl Pts',(-22.7429244249728,27.3995005528144,-23.6994660712205));
#65294=CARTESIAN_POINT('Ctrl Pts',(-22.6300145151427,27.3758192147366,-23.7053383681892));
#65295=CARTESIAN_POINT('Ctrl Pts',(-22.5179583003379,27.3471260160167,-23.7112106651579));
#65296=CARTESIAN_POINT('Ctrl Pts',(-22.4072350181661,27.3134958089443,-23.7170829621266));
#65297=CARTESIAN_POINT('Ctrl Pts',(-22.2966552245749,27.2799091839495,-23.7229476490648));
#65298=CARTESIAN_POINT('Ctrl Pts',(-22.1874053203775,27.2413983928989,-23.728812336003));
#65299=CARTESIAN_POINT('Ctrl Pts',(-22.0799547837233,27.1980893608728,-23.7346770229412));
#65300=CARTESIAN_POINT('Ctrl Pts',(-21.9726147532193,27.1548248694748,-23.740535678416));
#65301=CARTESIAN_POINT('Ctrl Pts',(-21.8670707905509,27.1067721060629,-23.7463943338908));
#65302=CARTESIAN_POINT('Ctrl Pts',(-21.7637769748103,27.0541067074065,-23.7522529893657));
#65303=CARTESIAN_POINT('Ctrl Pts',(-21.656448411647,26.9993841518915,-23.7583404890836));
#65304=CARTESIAN_POINT('Ctrl Pts',(-21.5515497994855,26.9396814000109,-23.7644279888015));
#65305=CARTESIAN_POINT('Ctrl Pts',(-21.4495677345764,26.8752506344242,-23.7705154885194));
#65306=CARTESIAN_POINT('Ctrl Pts',(-21.35153310257,26.8133137987677,-23.7763673586028));
#65307=CARTESIAN_POINT('Ctrl Pts',(-21.2561938157888,26.7470084006965,-23.7822192286862));
#65308=CARTESIAN_POINT('Ctrl Pts',(-21.1639560620088,26.6766047445402,-23.7880710987696));
#65309=CARTESIAN_POINT('Ctrl Pts',(-21.0717323522655,26.6062118079806,-23.7939220778525));
#65310=CARTESIAN_POINT('Ctrl Pts',(-20.9826095650749,26.5317221047876,-23.7997730569355));
#65311=CARTESIAN_POINT('Ctrl Pts',(-20.896962864663,26.4534478304686,-23.8056240360185));
#65312=CARTESIAN_POINT('Ctrl Pts',(-20.8113084637884,26.3751665185388,-23.8114755411608));
#65313=CARTESIAN_POINT('Ctrl Pts',(-20.7291310761429,26.2931002379528,-23.8173270463031));
#65314=CARTESIAN_POINT('Ctrl Pts',(-20.6507703490071,26.2075993423834,-23.8231785514454));
#65315=CARTESIAN_POINT('Ctrl Pts',(-20.5723835999794,26.1220700538275,-23.8290319997452));
#65316=CARTESIAN_POINT('Ctrl Pts',(-20.497816310822,26.033104186947,-23.834885448045));
#65317=CARTESIAN_POINT('Ctrl Pts',(-20.4273685779228,25.9410860288824,-23.8407388963448));
#65318=CARTESIAN_POINT('Ctrl Pts',(-20.3568407306543,25.8489632261913,-23.8465990012864));
#65319=CARTESIAN_POINT('Ctrl Pts',(-20.2904420418637,25.753781532499,-23.8524591062279));
#65320=CARTESIAN_POINT('Ctrl Pts',(-20.2284299580411,25.6559552146883,-23.8583192111694));
#65321=CARTESIAN_POINT('Ctrl Pts',(-20.1663761129612,25.5580630169754,-23.8641832625249));
#65322=CARTESIAN_POINT('Ctrl Pts',(-20.1087149602132,25.4575230065598,-23.8700473138803));
#65323=CARTESIAN_POINT('Ctrl Pts',(-20.0556577230711,25.3547735549977,-23.8759113652358));
#65324=CARTESIAN_POINT('Ctrl Pts',(-20.0025222901525,25.2518726712544,-23.8817840590324));
#65325=CARTESIAN_POINT('Ctrl Pts',(-19.9540044874834,25.1467562213898,-23.887656752829));
#65326=CARTESIAN_POINT('Ctrl Pts',(-19.9102672571527,25.0398820833349,-23.8935294466255));
#65327=CARTESIAN_POINT('Ctrl Pts',(-19.8982927351231,25.0106217321225,-23.8951372919488));
#65328=CARTESIAN_POINT('Ctrl Pts',(-19.8866762617299,24.9812297116053,-23.8967451372721));
#65329=CARTESIAN_POINT('Ctrl Pts',(-19.8754205211404,24.9517155865797,-23.8983529825954));
#65330=CARTESIAN_POINT('Ctrl Pts',(-19.8343114353426,24.8439218178553,-23.9042252795641));
#65331=CARTESIAN_POINT('Ctrl Pts',(-19.7978803703453,24.7341371539342,-23.9100975765328));
#65332=CARTESIAN_POINT('Ctrl Pts',(-19.7663233999043,24.6228052462924,-23.9159698735015));
#65333=CARTESIAN_POINT('Ctrl Pts',(-19.7348073247909,24.5116176159614,-23.9218345604396));
#65334=CARTESIAN_POINT('Ctrl Pts',(-19.7081528947946,24.3988871233872,-23.9276992473778));
#65335=CARTESIAN_POINT('Ctrl Pts',(-19.6865079398746,24.2850768162582,-23.933563934316));
#65336=CARTESIAN_POINT('Ctrl Pts',(-19.6648852454358,24.1713835559055,-23.9394225897908));
#65337=CARTESIAN_POINT('Ctrl Pts',(-19.648261855387,24.0566130935448,-23.9452812452656));
#65338=CARTESIAN_POINT('Ctrl Pts',(-19.6367354525663,23.941242392655,-23.9511399007404));
#65339=CARTESIAN_POINT('Ctrl Pts',(-19.624758818299,23.8213652105709,-23.9572274004583));
#65340=CARTESIAN_POINT('Ctrl Pts',(-19.6182855983226,23.7008403797738,-23.9633149001762));
#65341=CARTESIAN_POINT('Ctrl Pts',(-19.617366653036,23.580213597272,-23.9694023998941));
#65342=CARTESIAN_POINT('Ctrl Pts',(-19.6164832774827,23.4642559311546,-23.9752542699775));
#65343=CARTESIAN_POINT('Ctrl Pts',(-19.6207321951438,23.3482045110168,-23.9811061400609));
#65344=CARTESIAN_POINT('Ctrl Pts',(-19.630105556164,23.2325471803988,-23.9869580101443));
#65345=CARTESIAN_POINT('Ctrl Pts',(-19.6394774900048,23.116907459661,-23.9928089892272));
#65346=CARTESIAN_POINT('Ctrl Pts',(-19.6539722824479,23.0016621210552,-23.9986599683102));
#65347=CARTESIAN_POINT('Ctrl Pts',(-19.6735300703436,22.887295551446,-24.0045109473932));
#65348=CARTESIAN_POINT('Ctrl Pts',(-19.6930896166726,22.7729186991816,-24.0103624525354));
#65349=CARTESIAN_POINT('Ctrl Pts',(-19.7177129936886,22.65942118047,-24.0162139576777));
#65350=CARTESIAN_POINT('Ctrl Pts',(-19.7472890367221,22.54727812728,-24.02206546282));
#65351=CARTESIAN_POINT('Ctrl Pts',(-19.7768749013158,22.4350978338231,-24.0279189111198));
#65352=CARTESIAN_POINT('Ctrl Pts',(-19.8114165968919,22.3242732997676,-24.0337723594195));
#65353=CARTESIAN_POINT('Ctrl Pts',(-19.8507530310512,22.2152647247302,-24.0396258077193));
#65354=CARTESIAN_POINT('Ctrl Pts',(-19.8901341992779,22.1061321832724,-24.0454859126608));
#65355=CARTESIAN_POINT('Ctrl Pts',(-19.9343208490314,21.9988201118604,-24.0513460176024));
#65356=CARTESIAN_POINT('Ctrl Pts',(-19.9831036113743,21.8937690333578,-24.0572061225439));
#65357=CARTESIAN_POINT('Ctrl Pts',(-20.0319192258544,21.788647209529,-24.0630701738993));
#65358=CARTESIAN_POINT('Ctrl Pts',(-20.0853369260118,21.6857897764459,-24.0689342252548));
#65359=CARTESIAN_POINT('Ctrl Pts',(-20.1431020776351,21.5856113982032,-24.0747982766102));
#65360=CARTESIAN_POINT('Ctrl Pts',(-20.2009523635608,21.4852853770285,-24.0806709704068));
#65361=CARTESIAN_POINT('Ctrl Pts',(-20.2631626673428,21.3876466382453,-24.0865436642033));
#65362=CARTESIAN_POINT('Ctrl Pts',(-20.3294358457019,21.2930797701994,-24.0924163579999));
#65363=CARTESIAN_POINT('Ctrl Pts',(-20.3475803333228,21.2671889436375,-24.0940242033233));
#65364=CARTESIAN_POINT('Ctrl Pts',(-20.3660291370058,21.2415281765597,-24.0956320486467));
#65365=CARTESIAN_POINT('Ctrl Pts',(-20.3847756606335,21.216104897379,-24.0972398939701));
#65366=CARTESIAN_POINT('Ctrl Pts',(-20.4532431632402,21.1232520320611,-24.1031121909388));
#65367=CARTESIAN_POINT('Ctrl Pts',(-20.5259143079376,21.0332587008779,-24.1089844879075));
#65368=CARTESIAN_POINT('Ctrl Pts',(-20.6025218294725,20.9465296764003,-24.1148567848762));
#65369=CARTESIAN_POINT('Ctrl Pts',(-20.6790300737437,20.8599130458505,-24.1207214718144));
#65370=CARTESIAN_POINT('Ctrl Pts',(-20.7594642791921,20.7765526164585,-24.1265861587526));
#65371=CARTESIAN_POINT('Ctrl Pts',(-20.8435147843884,20.6968230569551,-24.1324508456908));
#65372=CARTESIAN_POINT('Ctrl Pts',(-20.9274788489016,20.6171754943126,-24.1383095011656));
#65373=CARTESIAN_POINT('Ctrl Pts',(-21.015051517496,20.5411516569819,-24.1441681566405));
#65374=CARTESIAN_POINT('Ctrl Pts',(-21.1058843145094,20.4690915461537,-24.1500268121153));
#65375=CARTESIAN_POINT('Ctrl Pts',(-21.2002651205788,20.3942167039267,-24.1561143118332));
#65376=CARTESIAN_POINT('Ctrl Pts',(-21.2981656331073,20.3236218948951,-24.1622018115511));
#65377=CARTESIAN_POINT('Ctrl Pts',(-21.3991542402479,20.2576448811326,-24.168289311269));
#65378=CARTESIAN_POINT('Ctrl Pts',(-21.4962338683834,20.1942216481273,-24.1741411813524));
#65379=CARTESIAN_POINT('Ctrl Pts',(-21.596166595405,20.1350656214916,-24.1799930514358));
#65380=CARTESIAN_POINT('Ctrl Pts',(-21.6985377471777,20.0804338971251,-24.1858449215192));
#65381=CARTESIAN_POINT('Ctrl Pts',(-21.800893312012,20.0258104909352,-24.1916959006022));
#65382=CARTESIAN_POINT('Ctrl Pts',(-21.9056861987896,19.9757102119016,-24.1975468796851));
#65383=CARTESIAN_POINT('Ctrl Pts',(-22.0124765261438,19.9303445277867,-24.2033978587681));
#65384=CARTESIAN_POINT('Ctrl Pts',(-22.1192764549758,19.8849747648604,-24.2092493639104));
#65385=CARTESIAN_POINT('Ctrl Pts',(-22.2280738008934,19.8443406047161,-24.2151008690527));
#65386=CARTESIAN_POINT('Ctrl Pts',(-22.3384087381831,19.8086053516238,-24.220952374195));
#65387=CARTESIAN_POINT('Ctrl Pts',(-22.4487803153041,19.7728582316317,-24.2268058224948));
#65388=CARTESIAN_POINT('Ctrl Pts',(-22.560690106032,19.7420133808265,-24.2326592707945));
#65389=CARTESIAN_POINT('Ctrl Pts',(-22.6736638594369,19.7161840268719,-24.2385127190943));
#65390=CARTESIAN_POINT('Ctrl Pts',(-22.786766088531,19.6903252993332,-24.2443728240359));
#65391=CARTESIAN_POINT('Ctrl Pts',(-22.9009342921154,19.6694935452655,-24.2502329289774));
#65392=CARTESIAN_POINT('Ctrl Pts',(-23.0156846781272,19.653750740352,-24.2560930339189));
#65393=CARTESIAN_POINT('Ctrl Pts',(-23.1305123413419,19.6379973336447,-24.2619570852744));
#65394=CARTESIAN_POINT('Ctrl Pts',(-23.2459225570346,19.627339738025,-24.2678211366298));
#65395=CARTESIAN_POINT('Ctrl Pts',(-23.361428820759,19.6217878689807,-24.2736851879853));
#65396=CARTESIAN_POINT('Ctrl Pts',(-23.4771053176591,19.6162278175896,-24.2795578817819));
#65397=CARTESIAN_POINT('Ctrl Pts',(-23.5928777332809,19.6157885124291,-24.2854305755784));
#65398=CARTESIAN_POINT('Ctrl Pts',(-23.7082618884572,19.6204278481777,-24.291303269375));
#65399=CARTESIAN_POINT('Ctrl Pts',(-23.7398521400037,19.6216980206991,-24.2929111146984));
#65400=CARTESIAN_POINT('Ctrl Pts',(-23.7714133343787,19.6233485763334,-24.2945189600217));
#65401=CARTESIAN_POINT('Ctrl Pts',(-23.8029356564525,19.6253779810286,-24.2961268053451));
#65402=CARTESIAN_POINT('Ctrl Pts',(-23.9180639176554,19.6327899297198,-24.3019991023138));
#65403=CARTESIAN_POINT('Ctrl Pts',(-24.0330586515679,19.6452841724555,-24.3078713992825));
#65404=CARTESIAN_POINT('Ctrl Pts',(-24.1474348480352,19.6628546512284,-24.3137436962512));
#65405=CARTESIAN_POINT('Ctrl Pts',(-24.2616628220351,19.6804023600562,-24.3196083831894));
#65406=CARTESIAN_POINT('Ctrl Pts',(-24.3752734478172,19.7030131606592,-24.3254730701276));
#65407=CARTESIAN_POINT('Ctrl Pts',(-24.487784125162,19.7306290540135,-24.3313377570658));
#65408=CARTESIAN_POINT('Ctrl Pts',(-24.6001790923184,19.7582165461502,-24.3371964125406));
#65409=CARTESIAN_POINT('Ctrl Pts',(-24.7114759620557,19.7907987945982,-24.3430550680155));
#65410=CARTESIAN_POINT('Ctrl Pts',(-24.8212003197991,19.8282664059931,-24.3489137234903));
#65411=CARTESIAN_POINT('Ctrl Pts',(-24.9352106076,19.8671975352902,-24.3550012232082));
#65412=CARTESIAN_POINT('Ctrl Pts',(-25.0475225822143,19.9114033920715,-24.3610887229261));
#65413=CARTESIAN_POINT('Ctrl Pts',(-25.1576187742416,19.9607034287679,-24.367176222644));
#65414=CARTESIAN_POINT('Ctrl Pts',(-25.2634534588044,20.0080952026033,-24.3730280927274));
#65415=CARTESIAN_POINT('Ctrl Pts',(-25.3672402919517,20.060193942344,-24.3788799628108));
#65416=CARTESIAN_POINT('Ctrl Pts',(-25.4685388256401,20.1167897469157,-24.3847318328942));
#65417=CARTESIAN_POINT('Ctrl Pts',(-25.5698219357058,20.1733769342615,-24.3905828119771));
#65418=CARTESIAN_POINT('Ctrl Pts',(-25.6686171388405,20.2344596234291,-24.3964337910601));
#65419=CARTESIAN_POINT('Ctrl Pts',(-25.7645087491411,20.2997820421346,-24.4022847701431));
#65420=CARTESIAN_POINT('Ctrl Pts',(-25.8604089810202,20.3651103339542,-24.4081362752854));
#65421=CARTESIAN_POINT('Ctrl Pts',(-25.953404759435,20.4346788803412,-24.4139877804276));
#65422=CARTESIAN_POINT('Ctrl Pts',(-26.0431101384716,20.5081890950887,-24.4198392855699));
#65423=CARTESIAN_POINT('Ctrl Pts',(-26.1328453067121,20.5817237209785,-24.4256927338697));
#65424=CARTESIAN_POINT('Ctrl Pts',(-26.2192875832983,20.6592023561018,-24.4315461821695));
#65425=CARTESIAN_POINT('Ctrl Pts',(-26.3020853551643,20.7402872095466,-24.4373996304693));
#65426=CARTESIAN_POINT('Ctrl Pts',(-26.3849772860759,20.8214642740766,-24.4432597354108));
#65427=CARTESIAN_POINT('Ctrl Pts',(-26.4642161442643,20.9062554531002,-24.4491198403524));
#65428=CARTESIAN_POINT('Ctrl Pts',(-26.5394882784282,20.9942872247216,-24.4549799452939));
#65429=CARTESIAN_POINT('Ctrl Pts',(-26.6148111036633,21.0823782802315,-24.4608439966494));
#65430=CARTESIAN_POINT('Ctrl Pts',(-26.6861616318421,21.1737139488348,-24.4667080480048));
#65431=CARTESIAN_POINT('Ctrl Pts',(-26.7532685446208,21.26789028592,-24.4725720993603));
#65432=CARTESIAN_POINT('Ctrl Pts',(-26.8204743595932,21.3622054201265,-24.4784447931568));
#65433=CARTESIAN_POINT('Ctrl Pts',(-26.88342385298,21.4593692327844,-24.4843174869534));
#65434=CARTESIAN_POINT('Ctrl Pts',(-26.9418907293289,21.5589516161254,-24.49019018075));
#65435=CARTESIAN_POINT('Ctrl Pts',(-26.9578979820419,21.5862156068744,-24.4917980260733));
#65436=CARTESIAN_POINT('Ctrl Pts',(-26.9735695054268,21.6136607645356,-24.4934058713966));
#65437=CARTESIAN_POINT('Ctrl Pts',(-26.9889012846137,21.6412780022556,-24.49501371672));
#65438=CARTESIAN_POINT('Ctrl Pts',(-27.0476041889497,21.7470199415403,-24.501169896577));
#65439=CARTESIAN_POINT('Ctrl Pts',(-27.1015037032677,21.8556120215365,-24.5073260764341));
#65440=CARTESIAN_POINT('Ctrl Pts',(-27.1503271994092,21.966601248464,-24.5134822562911));
#65441=CARTESIAN_POINT('Ctrl Pts',(-27.1990638964661,22.0773931572136,-24.5196274916067));
#65442=CARTESIAN_POINT('Ctrl Pts',(-27.2427424068359,22.1905734009645,-24.5257727269224));
#65443=CARTESIAN_POINT('Ctrl Pts',(-27.2811355030515,22.3056637425608,-24.531917962238));
#65444=CARTESIAN_POINT('Ctrl Pts',(-27.3194415615513,22.4204931726542,-24.5380492662145));
#65445=CARTESIAN_POINT('Ctrl Pts',(-27.3524859794983,22.537223732537,-24.5441805701909));
#65446=CARTESIAN_POINT('Ctrl Pts',(-27.3800895822657,22.655357473003,-24.5503118741674));
#65447=CARTESIAN_POINT('Ctrl Pts',(-27.4076555417525,22.773330113428,-24.5564348168297));
#65448=CARTESIAN_POINT('Ctrl Pts',(-27.4297953798824,22.8927017794769,-24.5625577594919));
#65449=CARTESIAN_POINT('Ctrl Pts',(-27.446379339963,23.0129584838122,-24.5686807021542));
#65450=CARTESIAN_POINT('Ctrl Pts',(-27.4629352965204,23.1330121237777,-24.5747933056715));
#65451=CARTESIAN_POINT('Ctrl Pts',(-27.4739540263127,23.253947471905,-24.5809059091889));
#65452=CARTESIAN_POINT('Ctrl Pts',(-27.4793567136677,23.3752401687067,-24.5870185127062));
#65453=CARTESIAN_POINT('Ctrl Pts',(-27.4819546633665,23.4335652770136,-24.5899578344592));
#65454=CARTESIAN_POINT('Ctrl Pts',(-27.4832547774517,23.4919728544158,-24.5928971562121));
#65455=CARTESIAN_POINT('Ctrl Pts',(-27.4832525287818,23.5504038899366,-24.5958364779651));
#65456=CARTESIAN_POINT('',(-27.4832509217898,23.5538111136364,-25.8458364779651));
#65457=CARTESIAN_POINT('Ctrl Pts',(-27.4832525287817,23.5504038905352,-24.5958364779952));
#65458=CARTESIAN_POINT('Ctrl Pts',(-27.4832478259376,23.6726054471124,-24.6019837196159));
#65459=CARTESIAN_POINT('Ctrl Pts',(-27.4775434726152,23.794689959441,-24.6081309612367));
#65460=CARTESIAN_POINT('Ctrl Pts',(-27.4661978260355,23.9161233445858,-24.6142782028574));
#65461=CARTESIAN_POINT('Ctrl Pts',(-27.4548350958917,24.0377395765178,-24.6204347006096));
#65462=CARTESIAN_POINT('Ctrl Pts',(-27.4378141573329,24.1587023794636,-24.6265911983618));
#65463=CARTESIAN_POINT('Ctrl Pts',(-27.415244682518,24.2784864735495,-24.632747696114));
#65464=CARTESIAN_POINT('Ctrl Pts',(-27.3926182231349,24.3985730046634,-24.6389197381077));
#65465=CARTESIAN_POINT('Ctrl Pts',(-27.3644152868304,24.5174745349927,-24.6450917801014));
#65466=CARTESIAN_POINT('Ctrl Pts',(-27.3307961618426,24.6346781218313,-24.651263822095));
#65467=CARTESIAN_POINT('Ctrl Pts',(-27.2971300334542,24.7520455727547,-24.6574444933128));
#65468=CARTESIAN_POINT('Ctrl Pts',(-27.2580327171207,24.8677100144452,-24.6636251645305));
#65469=CARTESIAN_POINT('Ctrl Pts',(-27.2137129937155,24.9811775622975,-24.6698058357483));
#65470=CARTESIAN_POINT('Ctrl Pts',(-27.1692929457998,25.0949019613957,-24.6760004978659));
#65471=CARTESIAN_POINT('Ctrl Pts',(-27.1196270025272,25.2064192089251,-24.6821951599836));
#65472=CARTESIAN_POINT('Ctrl Pts',(-27.0649708348363,25.3152579848183,-24.6883898221012));
#65473=CARTESIAN_POINT('Ctrl Pts',(-27.048763357561,25.3475325123143,-24.6902267574324));
#65474=CARTESIAN_POINT('Ctrl Pts',(-27.0321173672469,25.3795717027539,-24.6920636927636));
#65475=CARTESIAN_POINT('Ctrl Pts',(-27.0150402581779,25.4113637616877,-24.6939006280948));
#65476=CARTESIAN_POINT('Ctrl Pts',(-26.960448322296,25.5129963059227,-24.6997729250635));
#65477=CARTESIAN_POINT('Ctrl Pts',(-26.901289360933,25.6123950595346,-24.7056452220323));
#65478=CARTESIAN_POINT('Ctrl Pts',(-26.8377704677816,25.7091214068008,-24.711517519001));
#65479=CARTESIAN_POINT('Ctrl Pts',(-26.7743338900711,25.8057224044027,-24.7173822059392));
#65480=CARTESIAN_POINT('Ctrl Pts',(-26.7065488414596,25.8996575404238,-24.7232468928774));
#65481=CARTESIAN_POINT('Ctrl Pts',(-26.6346686561638,25.990511979194,-24.7291115798156));
#65482=CARTESIAN_POINT('Ctrl Pts',(-26.5628623951388,26.0812729798615,-24.7349702352904));
#65483=CARTESIAN_POINT('Ctrl Pts',(-26.4869696294465,26.1689592629559,-24.7408288907653));
#65484=CARTESIAN_POINT('Ctrl Pts',(-26.4072870360614,26.2531847988543,-24.7466875462401));
#65485=CARTESIAN_POINT('Ctrl Pts',(-26.3244919703955,26.3407002583695,-24.752775045958));
#65486=CARTESIAN_POINT('Ctrl Pts',(-26.2376052229308,26.4244787193873,-24.7588625456759));
#65487=CARTESIAN_POINT('Ctrl Pts',(-26.1470060826493,26.5041245660928,-24.7649500453938));
#65488=CARTESIAN_POINT('Ctrl Pts',(-26.0599137749427,26.5806875507666,-24.7708019154772));
#65489=CARTESIAN_POINT('Ctrl Pts',(-25.9693914621539,26.6534315972908,-24.7766537855606));
#65490=CARTESIAN_POINT('Ctrl Pts',(-25.8758131190781,26.7220433435868,-24.782505655644));
#65491=CARTESIAN_POINT('Ctrl Pts',(-25.782249024156,26.7906446431206,-24.788356634727));
#65492=CARTESIAN_POINT('Ctrl Pts',(-25.6856301574126,26.8551146490741,-24.79420761381));
#65493=CARTESIAN_POINT('Ctrl Pts',(-25.5863619232682,26.9151815867478,-24.800058592893));
#65494=CARTESIAN_POINT('Ctrl Pts',(-25.4870847639543,26.9752539250172,-24.8059100980353));
#65495=CARTESIAN_POINT('Ctrl Pts',(-25.3851581174088,27.0309221940169,-24.8117616031776));
#65496=CARTESIAN_POINT('Ctrl Pts',(-25.2810139680362,27.0819594632602,-24.8176131083199));
#65497=CARTESIAN_POINT('Ctrl Pts',(-25.1768352346587,27.1330136808696,-24.8234665566197));
#65498=CARTESIAN_POINT('Ctrl Pts',(-25.070437905208,27.1794336589788,-24.8293200049194));
#65499=CARTESIAN_POINT('Ctrl Pts',(-24.9622753524433,27.2210399885873,-24.8351734532192));
#65500=CARTESIAN_POINT('Ctrl Pts',(-24.853989795369,27.2626936336272,-24.8410335581608));
#65501=CARTESIAN_POINT('Ctrl Pts',(-24.7439353942383,27.2995225554008,-24.8468936631023));
#65502=CARTESIAN_POINT('Ctrl Pts',(-24.6325822424161,27.3313967232437,-24.8527537680438));
#65503=CARTESIAN_POINT('Ctrl Pts',(-24.5211541012155,27.3632923563437,-24.8586178193993));
#65504=CARTESIAN_POINT('Ctrl Pts',(-24.4084258688501,27.3902264956169,-24.8644818707548));
#65505=CARTESIAN_POINT('Ctrl Pts',(-24.2948777144468,27.4121202582238,-24.8703459221102));
#65506=CARTESIAN_POINT('Ctrl Pts',(-24.1811622127302,27.4340462878663,-24.8762186159068));
#65507=CARTESIAN_POINT('Ctrl Pts',(-24.0666247846745,27.4509170549587,-24.8820913097034));
#65508=CARTESIAN_POINT('Ctrl Pts',(-23.9517506829399,27.4627055006826,-24.8879640034999));
#65509=CARTESIAN_POINT('Ctrl Pts',(-23.920300075495,27.4659329799251,-24.8895718488232));
#65510=CARTESIAN_POINT('Ctrl Pts',(-23.8888242289008,27.4687798036578,-24.8911796941465));
#65511=CARTESIAN_POINT('Ctrl Pts',(-23.8573330766582,27.4712460969662,-24.8927875394698));
#65512=CARTESIAN_POINT('Ctrl Pts',(-23.7423186563169,27.4802536840202,-24.8986598364385));
#65513=CARTESIAN_POINT('Ctrl Pts',(-23.6267148906233,27.4842114973813,-24.9045321334072));
#65514=CARTESIAN_POINT('Ctrl Pts',(-23.5110027372644,27.4830566780556,-24.9104044303759));
#65515=CARTESIAN_POINT('Ctrl Pts',(-23.3954405376666,27.481903355284,-24.9162691173141));
#65516=CARTESIAN_POINT('Ctrl Pts',(-23.2797706392785,27.4756505797853,-24.9221338042523));
#65517=CARTESIAN_POINT('Ctrl Pts',(-23.1644789881933,27.4642872496208,-24.9279984911906));
#65518=CARTESIAN_POINT('Ctrl Pts',(-23.0493059073539,27.45293560593,-24.9338571466654));
#65519=CARTESIAN_POINT('Ctrl Pts',(-22.9345107089853,27.4364839021035,-24.9397158021402));
#65520=CARTESIAN_POINT('Ctrl Pts',(-22.8205785327678,27.4149730720814,-24.945574457615));
#65521=CARTESIAN_POINT('Ctrl Pts',(-22.7021960653973,27.3926220100922,-24.9516619573329));
#65522=CARTESIAN_POINT('Ctrl Pts',(-22.5847458700919,27.3648085414441,-24.9577494570508));
#65523=CARTESIAN_POINT('Ctrl Pts',(-22.4687658068485,27.3316379212019,-24.9638369567687));
#65524=CARTESIAN_POINT('Ctrl Pts',(-22.3572749988294,27.2997512404236,-24.9696888268521));
#65525=CARTESIAN_POINT('Ctrl Pts',(-22.2471430643954,27.262914540854,-24.9755406969355));
#65526=CARTESIAN_POINT('Ctrl Pts',(-22.1388357895518,27.2212730682753,-24.9813925670189));
#65527=CARTESIAN_POINT('Ctrl Pts',(-22.0305450054756,27.1796379359894,-24.9872435461019));
#65528=CARTESIAN_POINT('Ctrl Pts',(-21.9240787143339,27.1331996335984,-24.9930945251849));
#65529=CARTESIAN_POINT('Ctrl Pts',(-21.8198847030169,27.0821523288967,-24.9989455042679));
#65530=CARTESIAN_POINT('Ctrl Pts',(-21.7156813236557,27.031100434551,-25.0047970094102));
#65531=CARTESIAN_POINT('Ctrl Pts',(-21.6137510014951,26.9754388960015,-25.0106485145525));
#65532=CARTESIAN_POINT('Ctrl Pts',(-21.5145181628449,26.9154084834275,-25.0165000196948));
#65533=CARTESIAN_POINT('Ctrl Pts',(-21.4152523711293,26.8553581360602,-25.0223534679945));
#65534=CARTESIAN_POINT('Ctrl Pts',(-21.3186861976289,26.7909362436832,-25.0282069162943));
#65535=CARTESIAN_POINT('Ctrl Pts',(-21.2252156493426,26.7224272582351,-25.0340603645941));
#65536=CARTESIAN_POINT('Ctrl Pts',(-21.131638804746,26.653840363194,-25.0399204695356));
#65537=CARTESIAN_POINT('Ctrl Pts',(-21.0411649455847,26.5811573425102,-25.0457805744772));
#65538=CARTESIAN_POINT('Ctrl Pts',(-20.9541575742307,26.5047034065325,-25.0516406794187));
#65539=CARTESIAN_POINT('Ctrl Pts',(-20.8670916088577,26.4281979836139,-25.0575047307742));
#65540=CARTESIAN_POINT('Ctrl Pts',(-20.7834970770969,26.347916874439,-25.0633687821296));
#65541=CARTESIAN_POINT('Ctrl Pts',(-20.7036998961738,26.264221413832,-25.0692328334851));
#65542=CARTESIAN_POINT('Ctrl Pts',(-20.6237851101352,26.1804026028232,-25.0751055272817));
#65543=CARTESIAN_POINT('Ctrl Pts',(-20.5476791152681,26.0931597076787,-25.0809782210782));
#65544=CARTESIAN_POINT('Ctrl Pts',(-20.4756669762447,26.0028863531648,-25.0868509148748));
#65545=CARTESIAN_POINT('Ctrl Pts',(-20.4559512571966,25.9781710187883,-25.0884587601981));
#65546=CARTESIAN_POINT('Ctrl Pts',(-20.4365421471854,25.9532286898519,-25.0900666055214));
#65547=CARTESIAN_POINT('Ctrl Pts',(-20.417444910453,25.9280677911904,-25.0916744508447));
#65548=CARTESIAN_POINT('Ctrl Pts',(-20.3476965063314,25.8361732122785,-25.0975467478134));
#65549=CARTESIAN_POINT('Ctrl Pts',(-20.2818779953968,25.7410531904775,-25.1034190447821));
#65550=CARTESIAN_POINT('Ctrl Pts',(-20.2203022399947,25.6430783856081,-25.1092913417508));
#65551=CARTESIAN_POINT('Ctrl Pts',(-20.1588062818814,25.5452305483048,-25.115156028689));
#65552=CARTESIAN_POINT('Ctrl Pts',(-20.1015423631453,25.4445356318221,-25.1210207156272));
#65553=CARTESIAN_POINT('Ctrl Pts',(-20.0487824984981,25.3413964696929,-25.1268854025653));
#65554=CARTESIAN_POINT('Ctrl Pts',(-19.9960768940688,25.2383633797354,-25.1327440580401));
#65555=CARTESIAN_POINT('Ctrl Pts',(-19.9478663172968,25.1328914099305,-25.138602713515));
#65556=CARTESIAN_POINT('Ctrl Pts',(-19.9043785683351,25.0254108429612,-25.1444613689898));
#65557=CARTESIAN_POINT('Ctrl Pts',(-19.8591921495953,24.9137319903781,-25.1505488687077));
#65558=CARTESIAN_POINT('Ctrl Pts',(-19.8191052778004,24.7998848115582,-25.1566363684256));
#65559=CARTESIAN_POINT('Ctrl Pts',(-19.784320136228,24.6843787119661,-25.1627238681435));
#65560=CARTESIAN_POINT('Ctrl Pts',(-19.7508814276043,24.5733435218266,-25.1685757382269));
#65561=CARTESIAN_POINT('Ctrl Pts',(-19.7223417816217,24.460775879831,-25.1744276083103));
#65562=CARTESIAN_POINT('Ctrl Pts',(-19.6988307776489,24.347146171063,-25.1802794783937));
#65563=CARTESIAN_POINT('Ctrl Pts',(-19.6753233534402,24.2335337634515,-25.1861304574766));
#65564=CARTESIAN_POINT('Ctrl Pts',(-19.6568431326065,24.118860015295,-25.1919814365596));
#65565=CARTESIAN_POINT('Ctrl Pts',(-19.6434688063217,24.0036066131414,-25.1978324156425));
#65566=CARTESIAN_POINT('Ctrl Pts',(-19.6300932775564,23.8883428485979,-25.2036839207848));
#65567=CARTESIAN_POINT('Ctrl Pts',(-19.6218246035801,23.7724997371064,-25.2095354259271));
#65568=CARTESIAN_POINT('Ctrl Pts',(-19.6186896408146,23.6565645021312,-25.2153869310694));
#65569=CARTESIAN_POINT('Ctrl Pts',(-19.6155536369961,23.5405907675882,-25.2212403793691));
#65570=CARTESIAN_POINT('Ctrl Pts',(-19.6175547454316,23.424525261744,-25.2270938276689));
#65571=CARTESIAN_POINT('Ctrl Pts',(-19.624667710503,23.3088549102624,-25.2329472759687));
#65572=CARTESIAN_POINT('Ctrl Pts',(-19.6317887645602,23.1930530164737,-25.2388073809102));
#65573=CARTESIAN_POINT('Ctrl Pts',(-19.6440332530191,23.0776475868375,-25.2446674858517));
#65574=CARTESIAN_POINT('Ctrl Pts',(-19.6613240593988,22.9631202319782,-25.2505275907932));
#65575=CARTESIAN_POINT('Ctrl Pts',(-19.6786265100544,22.8485157501134,-25.2563916421487));
#65576=CARTESIAN_POINT('Ctrl Pts',(-19.7009819659387,22.7347909251069,-25.2622556935041));
#65577=CARTESIAN_POINT('Ctrl Pts',(-19.7282626020786,22.6224152733793,-25.2681197448595));
#65578=CARTESIAN_POINT('Ctrl Pts',(-19.7555834444305,22.5098740023734,-25.2739924386561));
#65579=CARTESIAN_POINT('Ctrl Pts',(-19.7878438393103,22.3986862686524,-25.2798651324526));
#65580=CARTESIAN_POINT('Ctrl Pts',(-19.8248667131377,22.2893046727808,-25.2857378262492));
#65581=CARTESIAN_POINT('Ctrl Pts',(-19.8350029566753,22.2593578215597,-25.2873456715727));
#65582=CARTESIAN_POINT('Ctrl Pts',(-19.8454959097274,22.2295462254831,-25.2889535168961));
#65583=CARTESIAN_POINT('Ctrl Pts',(-19.8563413298849,22.1998788674265,-25.2905613622195));
#65584=CARTESIAN_POINT('Ctrl Pts',(-19.895951811681,22.0915254491932,-25.2964336591882));
#65585=CARTESIAN_POINT('Ctrl Pts',(-19.9404001865646,21.9847348274171,-25.302305956157));
#65586=CARTESIAN_POINT('Ctrl Pts',(-19.9895437275704,21.8799705757852,-25.3081782531257));
#65587=CARTESIAN_POINT('Ctrl Pts',(-20.03862358245,21.7753420903031,-25.3140429400639));
#65588=CARTESIAN_POINT('Ctrl Pts',(-20.0923863295045,21.6727351235627,-25.3199076270021));
#65589=CARTESIAN_POINT('Ctrl Pts',(-20.150640093607,21.5725962747065,-25.3257723139403));
#65590=CARTESIAN_POINT('Ctrl Pts',(-20.2088339473598,21.4725604123875,-25.3316309694151));
#65591=CARTESIAN_POINT('Ctrl Pts',(-20.2715094246548,21.3749879743063,-25.3374896248899));
#65592=CARTESIAN_POINT('Ctrl Pts',(-20.3384276570915,21.2803031985849,-25.3433482803647));
#65593=CARTESIAN_POINT('Ctrl Pts',(-20.407959774628,21.1819199521265,-25.3494357800826));
#65594=CARTESIAN_POINT('Ctrl Pts',(-20.482072662717,21.0866549678214,-25.3555232798005));
#65595=CARTESIAN_POINT('Ctrl Pts',(-20.560447038627,20.9949537011021,-25.3616107795185));
#65596=CARTESIAN_POINT('Ctrl Pts',(-20.6357877674888,20.9068019271077,-25.3674626496019));
#65597=CARTESIAN_POINT('Ctrl Pts',(-20.7150659248526,20.8219434615175,-25.3733145196852));
#65598=CARTESIAN_POINT('Ctrl Pts',(-20.797955810997,20.7407415847072,-25.3791663897686));
#65599=CARTESIAN_POINT('Ctrl Pts',(-20.8808330764026,20.659552071621,-25.3850173688516));
#65600=CARTESIAN_POINT('Ctrl Pts',(-20.9673206819587,20.5820183295239,-25.3908683479346));
#65601=CARTESIAN_POINT('Ctrl Pts',(-21.0570559126059,20.5084669346202,-25.3967193270176));
#65602=CARTESIAN_POINT('Ctrl Pts',(-21.1467992113139,20.4349089267383,-25.4025708321598));
#65603=CARTESIAN_POINT('Ctrl Pts',(-21.2397903958381,20.3653342398889,-25.4084223373021));
#65604=CARTESIAN_POINT('Ctrl Pts',(-21.3356340739377,20.3000288337675,-25.4142738424444));
#65605=CARTESIAN_POINT('Ctrl Pts',(-21.4315095796365,20.2347017411422,-25.4201272907442));
#65606=CARTESIAN_POINT('Ctrl Pts',(-21.5302391210217,20.1736469809691,-25.425980739044));
#65607=CARTESIAN_POINT('Ctrl Pts',(-21.6313993876304,20.1171065092366,-25.4318341873438));
#65608=CARTESIAN_POINT('Ctrl Pts',(-21.7326746954286,20.0605017387102,-25.4376942922853));
#65609=CARTESIAN_POINT('Ctrl Pts',(-21.8363858847755,20.0084217051899,-25.4435543972268));
#65610=CARTESIAN_POINT('Ctrl Pts',(-21.9420860838447,19.961061860246,-25.4494145021684));
#65611=CARTESIAN_POINT('Ctrl Pts',(-22.0478574653824,19.9136701214106,-25.4552785535238));
#65612=CARTESIAN_POINT('Ctrl Pts',(-22.1556201403844,19.871005052478,-25.4611426048793));
#65613=CARTESIAN_POINT('Ctrl Pts',(-22.2649100019915,19.833212905683,-25.4670066562347));
#65614=CARTESIAN_POINT('Ctrl Pts',(-22.3743609350382,19.7953650608077,-25.4728793500313));
#65615=CARTESIAN_POINT('Ctrl Pts',(-22.4853431520009,19.7624045886343,-25.4787520438278));
#65616=CARTESIAN_POINT('Ctrl Pts',(-22.597380156654,19.7344271639808,-25.4846247376244));
#65617=CARTESIAN_POINT('Ctrl Pts',(-22.6280540143783,19.7267674131157,-25.4862325829477));
#65618=CARTESIAN_POINT('Ctrl Pts',(-22.6588068962948,19.7194808790895,-25.4878404282711));
#65619=CARTESIAN_POINT('Ctrl Pts',(-22.6896289517575,19.7125688483173,-25.4894482735945));
#65620=CARTESIAN_POINT('Ctrl Pts',(-22.8021996451161,19.6873241952643,-25.4953205705632));
#65621=CARTESIAN_POINT('Ctrl Pts',(-22.9160706179009,19.6669945005739,-25.5011928675319));
#65622=CARTESIAN_POINT('Ctrl Pts',(-23.0307747078158,19.6517102668856,-25.5070651645006));
#65623=CARTESIAN_POINT('Ctrl Pts',(-23.1453301503398,19.6364458403504,-25.5129298514388));
#65624=CARTESIAN_POINT('Ctrl Pts',(-23.2607161569714,19.6262139261508,-25.518794538377));
#65625=CARTESIAN_POINT('Ctrl Pts',(-23.3764532797184,19.6210945022924,-25.5246592253152));
#65626=CARTESIAN_POINT('Ctrl Pts',(-23.4920713740798,19.6159803434409,-25.5305178807901));
#65627=CARTESIAN_POINT('Ctrl Pts',(-23.6080394558122,19.6159682349018,-25.5363765362649));
#65628=CARTESIAN_POINT('Ctrl Pts',(-23.7238714877685,19.6210865313715,-25.5422351917397));
#65629=CARTESIAN_POINT('Ctrl Pts',(-23.8442280209165,19.6264047530094,-25.5483226914576));
#65630=CARTESIAN_POINT('Ctrl Pts',(-23.9644372084721,19.6372624066569,-25.5544101911755));
#65631=CARTESIAN_POINT('Ctrl Pts',(-24.0839516954544,19.6536316619403,-25.5604976908934));
#65632=CARTESIAN_POINT('Ctrl Pts',(-24.1988401198184,19.6693673103542,-25.5663495609768));
#65633=CARTESIAN_POINT('Ctrl Pts',(-24.3130861755907,19.6901957562358,-25.5722014310603));
#65634=CARTESIAN_POINT('Ctrl Pts',(-24.4262081743892,19.7160393513884,-25.5780533011437));
#65635=CARTESIAN_POINT('Ctrl Pts',(-24.5393129493348,19.7418790116186,-25.5839042802266));
#65636=CARTESIAN_POINT('Ctrl Pts',(-24.6512936047144,19.7727322107913,-25.5897552593096));
#65637=CARTESIAN_POINT('Ctrl Pts',(-24.7616793236217,19.8084703189244,-25.5956062383926));
#65638=CARTESIAN_POINT('Ctrl Pts',(-24.8720749672676,19.8442116402574,-25.6014577435349));
#65639=CARTESIAN_POINT('Ctrl Pts',(-24.9808749960669,19.8848386163045,-25.6073092486772));
#65640=CARTESIAN_POINT('Ctrl Pts',(-25.0876251010621,19.9301731702775,-25.6131607538195));
#65641=CARTESIAN_POINT('Ctrl Pts',(-25.1944106554432,19.975522778869,-25.6190142021193));
#65642=CARTESIAN_POINT('Ctrl Pts',(-25.2991445521298,20.0255829123766,-25.6248676504191));
#65643=CARTESIAN_POINT('Ctrl Pts',(-25.4013944122385,20.0801282200744,-25.6307210987189));
#65644=CARTESIAN_POINT('Ctrl Pts',(-25.5037605526413,20.1347355576314,-25.6365812036604));
#65645=CARTESIAN_POINT('Ctrl Pts',(-25.603636653125,20.193838055374,-25.642441308602));
#65646=CARTESIAN_POINT('Ctrl Pts',(-25.7006167238381,20.2571654023966,-25.6483014135435));
#65647=CARTESIAN_POINT('Ctrl Pts',(-25.797662104559,20.320535396424,-25.654165464899));
#65648=CARTESIAN_POINT('Ctrl Pts',(-25.8918072371198,20.3881356645135,-25.6600295162544));
#65649=CARTESIAN_POINT('Ctrl Pts',(-25.9826782076292,20.4596548013106,-25.6658935676099));
#65650=CARTESIAN_POINT('Ctrl Pts',(-26.0736831038095,20.5312793430387,-25.6717662614065));
#65651=CARTESIAN_POINT('Ctrl Pts',(-26.1614038952065,20.6068340117535,-25.677638955203));
#65652=CARTESIAN_POINT('Ctrl Pts',(-26.2455025225805,20.6859696394806,-25.6835116489996));
#65653=CARTESIAN_POINT('Ctrl Pts',(-26.2685273199561,20.7076356505738,-25.6851194943229));
#65654=CARTESIAN_POINT('Ctrl Pts',(-26.2912808396691,20.7295698855689,-25.6867273396461));
#65655=CARTESIAN_POINT('Ctrl Pts',(-26.3137566747453,20.7517647523142,-25.6883351849694));
#65656=CARTESIAN_POINT('Ctrl Pts',(-26.3946862692477,20.8316826534574,-25.6941246147989));
#65657=CARTESIAN_POINT('Ctrl Pts',(-26.4723004131786,20.9152665873004,-25.6999140446284));
#65658=CARTESIAN_POINT('Ctrl Pts',(-26.546241312436,21.0022061770002,-25.7057034744579));
#65659=CARTESIAN_POINT('Ctrl Pts',(-26.6208137127709,21.0898882846451,-25.711542349604));
#65660=CARTESIAN_POINT('Ctrl Pts',(-26.6916494610823,21.1809833960116,-25.7173812247501));
#65661=CARTESIAN_POINT('Ctrl Pts',(-26.7584167211044,21.2751324175494,-25.7232200998963));
#65662=CARTESIAN_POINT('Ctrl Pts',(-26.824453427439,21.3682512797722,-25.7289950872662));
#65663=CARTESIAN_POINT('Ctrl Pts',(-26.8865099624587,21.4643572122828,-25.7347700746361));
#65664=CARTESIAN_POINT('Ctrl Pts',(-26.94430404516,21.5630677582168,-25.7405450620059));
#65665=CARTESIAN_POINT('Ctrl Pts',(-27.0020609439112,21.6617147950882,-25.7463163338252));
#65666=CARTESIAN_POINT('Ctrl Pts',(-27.0555606251468,21.7629627491363,-25.7520876056444));
#65667=CARTESIAN_POINT('Ctrl Pts',(-27.1045639607166,21.8664000246375,-25.7578588774636));
#65668=CARTESIAN_POINT('Ctrl Pts',(-27.1535484216892,21.9697974592405,-25.7636279263642));
#65669=CARTESIAN_POINT('Ctrl Pts',(-27.1980397978055,22.0753821543431,-25.7693969752647));
#65670=CARTESIAN_POINT('Ctrl Pts',(-27.237845209806,22.182718531994,-25.7751660241652));
#65671=CARTESIAN_POINT('Ctrl Pts',(-27.2784796739708,22.2922904713871,-25.7810552286486));
#65672=CARTESIAN_POINT('Ctrl Pts',(-27.3142306032938,22.4036874607722,-25.7869444331319));
#65673=CARTESIAN_POINT('Ctrl Pts',(-27.3449451319187,22.5164261101894,-25.7928336376152));
#65674=CARTESIAN_POINT('Ctrl Pts',(-27.3750434035268,22.6269027687224,-25.7986046809628));
#65675=CARTESIAN_POINT('Ctrl Pts',(-27.4003054201884,22.7386673181903,-25.8043757243104));
#65676=CARTESIAN_POINT('Ctrl Pts',(-27.4206385093575,22.8512522570825,-25.810146767658));
#65677=CARTESIAN_POINT('Ctrl Pts',(-27.4415960733654,22.9672949323262,-25.8160950527092));
#65678=CARTESIAN_POINT('Ctrl Pts',(-27.4573169711912,23.0842087251304,-25.8220433377603));
#65679=CARTESIAN_POINT('Ctrl Pts',(-27.4677572464468,23.2014749379599,-25.8279916228115));
#65680=CARTESIAN_POINT('Ctrl Pts',(-27.4781975217024,23.3187411507893,-25.8339399078627));
#65681=CARTESIAN_POINT('Ctrl Pts',(-27.4833571923491,23.4363592900354,-25.8398881929139));
#65682=CARTESIAN_POINT('Ctrl Pts',(-27.4832509217898,23.5538111136364,-25.8458364779651));
#65683=CARTESIAN_POINT('',(-27.4887593445795,23.5484574312381,-27.0958364779651));
#65684=CARTESIAN_POINT('Ctrl Pts',(-27.4842361821344,23.5538120051012,-25.8458364779651));
#65685=CARTESIAN_POINT('Ctrl Pts',(-27.4867683033416,23.8262759091763,-25.8596316840915));
#65686=CARTESIAN_POINT('Ctrl Pts',(-27.3365065170297,25.4053452407083,-25.9397225273423));
#65687=CARTESIAN_POINT('Ctrl Pts',(-25.2023113590138,27.898982514481,-26.0861090077196));
#65688=CARTESIAN_POINT('Ctrl Pts',(-20.7846008650191,27.2908302532138,-26.2849959190938));
#65689=CARTESIAN_POINT('Ctrl Pts',(-18.908289764109,23.2454042145606,-26.483882830469));
#65690=CARTESIAN_POINT('Ctrl Pts',(-21.297548873069,19.4801079324787,-26.6827697418437));
#65691=CARTESIAN_POINT('Ctrl Pts',(-25.7568516465323,19.4549294457212,-26.8816566532187));
#65692=CARTESIAN_POINT('Ctrl Pts',(-27.4402597520929,22.0427902655866,-27.0193455652591));
#65693=CARTESIAN_POINT('Ctrl Pts',(-27.4893282421489,23.4480765207078,-27.0907388401746));
#65694=CARTESIAN_POINT('Ctrl Pts',(-27.4887593445795,23.5484574312381,-27.0958364779651));
#65695=CARTESIAN_POINT('',(-27.4787032760536,23.5475666446788,-28.3458364779651));
#65696=CARTESIAN_POINT('Ctrl Pts',(-27.4887593445795,23.5484574312381,-27.0958364779651));
#65697=CARTESIAN_POINT('Ctrl Pts',(-27.4819296335434,24.753547150884,-27.1570344772995));
#65698=CARTESIAN_POINT('Ctrl Pts',(-26.2449208629262,27.2762265169125,-27.2845281137589));
#65699=CARTESIAN_POINT('Ctrl Pts',(-21.9474057953528,27.9173606333923,-27.4783173873434));
#65700=CARTESIAN_POINT('Ctrl Pts',(-19.0097246028294,24.5623577432724,-27.6772042987183));
#65701=CARTESIAN_POINT('Ctrl Pts',(-20.244403603648,20.2773159760852,-27.8760912100932));
#65702=CARTESIAN_POINT('Ctrl Pts',(-24.5168774795743,18.9998254042427,-28.0749781214681));
#65703=CARTESIAN_POINT('Ctrl Pts',(-27.1812473048433,21.2860900718832,-28.2315598774252));
#65704=CARTESIAN_POINT('Ctrl Pts',(-27.4816774754266,23.0720448481154,-28.3218459962577));
#65705=CARTESIAN_POINT('Ctrl Pts',(-27.4787032760536,23.5475666446788,-28.3458364779651));
#65706=CARTESIAN_POINT('',(-27.482435324374,23.5530675880075,-29.5958365176789));
#65707=CARTESIAN_POINT('Ctrl Pts',(-27.4787032760536,23.5475666446788,-28.3458364779651));
#65708=CARTESIAN_POINT('Ctrl Pts',(-27.4734585307311,24.3861085194697,-28.3881416333826));
#65709=CARTESIAN_POINT('Ctrl Pts',(-26.7990027243226,26.5464152178334,-28.4967424259252));
#65710=CARTESIAN_POINT('Ctrl Pts',(-23.2394306216868,28.1918191392488,-28.6716388555926));
#65711=CARTESIAN_POINT('Ctrl Pts',(-19.4772122483696,25.7977163651147,-28.8705257669676));
#65712=CARTESIAN_POINT('Ctrl Pts',(-19.4577725585646,21.3383848815767,-29.0694126783425));
#65713=CARTESIAN_POINT('Ctrl Pts',(-23.1989749789817,18.9115722330461,-29.2682995897174));
#65714=CARTESIAN_POINT('Ctrl Pts',(-26.7845713929707,20.531216075928,-29.4437741895916));
#65715=CARTESIAN_POINT('Ctrl Pts',(-27.4733603952322,22.703195175,-29.5529531523408));
#65716=CARTESIAN_POINT('Ctrl Pts',(-27.4789478007187,23.5530643040686,-29.5958364779651));
#65717=CARTESIAN_POINT('',(-27.484770051487,23.5518598122456,-30.8458364779651));
#65718=CARTESIAN_POINT('Ctrl Pts',(-27.4832515237015,23.5530683565611,-29.5958365269733));
#65719=CARTESIAN_POINT('Ctrl Pts',(-27.4831563204269,23.6860433818375,-29.6025389720551));
#65720=CARTESIAN_POINT('Ctrl Pts',(-27.4763132956741,23.81874838759,-29.6092414171368));
#65721=CARTESIAN_POINT('Ctrl Pts',(-27.462828282249,23.950552414495,-29.6159438622185));
#65722=CARTESIAN_POINT('Ctrl Pts',(-27.4492748427458,24.0830252455284,-29.6226803170574));
#65723=CARTESIAN_POINT('Ctrl Pts',(-27.4290119542124,24.2145877774824,-29.6294167718962));
#65724=CARTESIAN_POINT('Ctrl Pts',(-27.4021964834553,24.344618185843,-29.6361532267351));
#65725=CARTESIAN_POINT('Ctrl Pts',(-27.3752149427135,24.4754538811259,-29.6429314008844));
#65726=CARTESIAN_POINT('Ctrl Pts',(-27.3415995030298,24.6047382666682,-29.6497095750338));
#65727=CARTESIAN_POINT('Ctrl Pts',(-27.3015582735726,24.7318591629173,-29.6564877491832));
#65728=CARTESIAN_POINT('Ctrl Pts',(-27.282682898258,24.7917837621254,-29.6596829702778));
#65729=CARTESIAN_POINT('Ctrl Pts',(-27.2623802904493,24.8512279175483,-29.6628781913724));
#65730=CARTESIAN_POINT('Ctrl Pts',(-27.240675848985,24.9101292684599,-29.6660734124671));
#65731=CARTESIAN_POINT('Ctrl Pts',(-27.200786613767,25.0183803766505,-29.6719457094357));
#65732=CARTESIAN_POINT('Ctrl Pts',(-27.156063523878,25.1250562415859,-29.6778180064044));
#65733=CARTESIAN_POINT('Ctrl Pts',(-27.1066504989764,25.2296936584715,-29.683690303373));
#65734=CARTESIAN_POINT('Ctrl Pts',(-27.0573015094307,25.3341954735751,-29.6895549903112));
#65735=CARTESIAN_POINT('Ctrl Pts',(-27.0032748462921,25.4366637236064,-29.6954196772494));
#65736=CARTESIAN_POINT('Ctrl Pts',(-26.9447635335279,25.5366523047585,-29.7012843641875));
#65737=CARTESIAN_POINT('Ctrl Pts',(-26.8863123959861,25.6365380539142,-29.7071430196623));
#65738=CARTESIAN_POINT('Ctrl Pts',(-26.8233859902127,25.733948851999,-29.7130016751371));
#65739=CARTESIAN_POINT('Ctrl Pts',(-26.756224275739,25.8284610771057,-29.7188603306119));
#65740=CARTESIAN_POINT('Ctrl Pts',(-26.6864391655421,25.9266650329714,-29.7249478303298));
#65741=CARTESIAN_POINT('Ctrl Pts',(-26.6120813258812,26.0217389468308,-29.7310353300477));
#65742=CARTESIAN_POINT('Ctrl Pts',(-26.5334711849622,26.1132381865104,-29.7371228297656));
#65743=CARTESIAN_POINT('Ctrl Pts',(-26.4579038168786,26.2011957533512,-29.742974699849));
#65744=CARTESIAN_POINT('Ctrl Pts',(-26.378407509792,26.2858498883758,-29.7488265699324));
#65745=CARTESIAN_POINT('Ctrl Pts',(-26.2953088973713,26.3668381507116,-29.7546784400158));
#65746=CARTESIAN_POINT('Ctrl Pts',(-26.2122229374701,26.447814081848,-29.7605294190987));
#65747=CARTESIAN_POINT('Ctrl Pts',(-26.1255360587556,26.5251249616578,-29.7663803981817));
#65748=CARTESIAN_POINT('Ctrl Pts',(-26.0356118156413,26.59844514859,-29.7722313772646));
#65749=CARTESIAN_POINT('Ctrl Pts',(-25.9456794874721,26.6717719277126,-29.7780828824069));
#65750=CARTESIAN_POINT('Ctrl Pts',(-25.8525095366855,26.7411070394505,-29.7839343875492));
#65751=CARTESIAN_POINT('Ctrl Pts',(-25.7564980902279,26.8061655427328,-29.7897858926914));
#65752=CARTESIAN_POINT('Ctrl Pts',(-25.660454760459,26.8712456505278,-29.7956393409912));
#65753=CARTESIAN_POINT('Ctrl Pts',(-25.5615684007677,26.9320460941839,-29.8014927892909));
#65754=CARTESIAN_POINT('Ctrl Pts',(-25.4602629429715,26.9883260080487,-29.8073462375907));
#65755=CARTESIAN_POINT('Ctrl Pts',(-25.3588422788718,27.0446699243964,-29.8132063425322));
#65756=CARTESIAN_POINT('Ctrl Pts',(-25.2549973872521,27.0964828491503,-29.8190664474737));
#65757=CARTESIAN_POINT('Ctrl Pts',(-25.14917564152,27.1435704815652,-29.8249265524152));
#65758=CARTESIAN_POINT('Ctrl Pts',(-25.0432826314653,27.1906898245533,-29.8307906037707));
#65759=CARTESIAN_POINT('Ctrl Pts',(-24.9354105002458,27.2330773880195,-29.8366546551261));
#65760=CARTESIAN_POINT('Ctrl Pts',(-24.8260237296135,27.2705881147511,-29.8425187064815));
#65761=CARTESIAN_POINT('Ctrl Pts',(-24.716475744717,27.3081541248061,-29.848391400278));
#65762=CARTESIAN_POINT('Ctrl Pts',(-24.6054090603038,27.3408288370644,-29.8542640940746));
#65763=CARTESIAN_POINT('Ctrl Pts',(-24.4933004172732,27.3685178034511,-29.8601367878711));
#65764=CARTESIAN_POINT('Ctrl Pts',(-24.4626069461535,27.3760985792696,-29.8617446331948));
#65765=CARTESIAN_POINT('Ctrl Pts',(-24.4318354117046,27.3833059360893,-29.8633524785185));
#65766=CARTESIAN_POINT('Ctrl Pts',(-24.400995667851,27.3901386128537,-29.8649603238421));
#65767=CARTESIAN_POINT('Ctrl Pts',(-24.2883603716054,27.4150934430608,-29.8708326208108));
#65768=CARTESIAN_POINT('Ctrl Pts',(-24.1744374505689,27.4351299844708,-29.8767049177795));
#65769=CARTESIAN_POINT('Ctrl Pts',(-24.0596944013836,27.4501189372788,-29.8825772147483));
#65770=CARTESIAN_POINT('Ctrl Pts',(-23.9451000500774,27.4650884655943,-29.8884419016865));
#65771=CARTESIAN_POINT('Ctrl Pts',(-23.8296880903085,27.4750233605025,-29.8943065886247));
#65772=CARTESIAN_POINT('Ctrl Pts',(-23.7139381743318,27.4798448782862,-29.9001712755629));
#65773=CARTESIAN_POINT('Ctrl Pts',(-23.5983072998975,27.4846614374407,-29.9060299310377));
#65774=CARTESIAN_POINT('Ctrl Pts',(-23.4823395711252,27.4843750623702,-29.9118885865125));
#65775=CARTESIAN_POINT('Ctrl Pts',(-23.3665210965324,27.4789586494553,-29.9177472419874));
#65776=CARTESIAN_POINT('Ctrl Pts',(-23.2461786503104,27.4733306666812,-29.9238347417053));
#65777=CARTESIAN_POINT('Ctrl Pts',(-23.1259978068178,27.4621636494904,-29.9299222414232));
#65778=CARTESIAN_POINT('Ctrl Pts',(-23.0065258475916,27.4454868369697,-29.9360097411411));
#65779=CARTESIAN_POINT('Ctrl Pts',(-22.8916783048566,27.429455535976,-29.9418616112245));
#65780=CARTESIAN_POINT('Ctrl Pts',(-22.7774862366438,27.4083331077393,-29.9477134813079));
#65781=CARTESIAN_POINT('Ctrl Pts',(-22.6644311298854,27.382198439989,-29.9535653513913));
#65782=CARTESIAN_POINT('Ctrl Pts',(-22.551393236795,27.3560677514795,-29.9594163304742));
#65783=CARTESIAN_POINT('Ctrl Pts',(-22.4394923636065,27.3249264339408,-29.9652673095572));
#65784=CARTESIAN_POINT('Ctrl Pts',(-22.3291989945931,27.2889043287372,-29.9711182886402));
#65785=CARTESIAN_POINT('Ctrl Pts',(-22.2188957091444,27.2528789847997,-29.9769697937825));
#65786=CARTESIAN_POINT('Ctrl Pts',(-22.1102006081625,27.2119721091923,-29.9828212989247));
#65787=CARTESIAN_POINT('Ctrl Pts',(-22.0035675407585,27.1663629474329,-29.988672804067));
#65788=CARTESIAN_POINT('Ctrl Pts',(-21.896899062834,27.1207386398638,-29.9945262523668));
#65789=CARTESIAN_POINT('Ctrl Pts',(-21.7922943599572,27.070409103625,-30.0003797006666));
#65790=CARTESIAN_POINT('Ctrl Pts',(-21.690185229562,27.0156008015711,-30.0062331489663));
#65791=CARTESIAN_POINT('Ctrl Pts',(-21.5879599789131,26.9607301705764,-30.0120932539079));
#65792=CARTESIAN_POINT('Ctrl Pts',(-21.4882363297693,26.901370803256,-30.0179533588494));
#65793=CARTESIAN_POINT('Ctrl Pts',(-21.3914195749,26.837794054574,-30.023813463791));
#65794=CARTESIAN_POINT('Ctrl Pts',(-21.2945376200058,26.7741744909309,-30.0296775151464));
#65795=CARTESIAN_POINT('Ctrl Pts',(-21.200566791724,26.7063321320196,-30.0355415665018));
#65796=CARTESIAN_POINT('Ctrl Pts',(-21.1098802011991,26.6345793445585,-30.0414056178573));
#65797=CARTESIAN_POINT('Ctrl Pts',(-21.0190599567425,26.5627208078119,-30.0472783116538));
#65798=CARTESIAN_POINT('Ctrl Pts',(-20.9315339217186,26.4869406098649,-30.0531510054504));
#65799=CARTESIAN_POINT('Ctrl Pts',(-20.8476392555443,26.4075887876463,-30.059023699247));
#65800=CARTESIAN_POINT('Ctrl Pts',(-20.8246702993324,26.385863586117,-30.0606315445703));
#65801=CARTESIAN_POINT('Ctrl Pts',(-20.8019733102506,26.3638708598002,-30.0622393898936));
#65802=CARTESIAN_POINT('Ctrl Pts',(-20.7795546757109,26.3416182173129,-30.0638472352169));
#65803=CARTESIAN_POINT('Ctrl Pts',(-20.6976756057894,26.2603453963959,-30.0697195321856));
#65804=CARTESIAN_POINT('Ctrl Pts',(-20.6192383589675,26.1753307315423,-30.0755918291543));
#65805=CARTESIAN_POINT('Ctrl Pts',(-20.5446044190939,26.0868976434949,-30.0814641261231));
#65806=CARTESIAN_POINT('Ctrl Pts',(-20.4700671988791,25.9985791577064,-30.0873288130613));
#65807=CARTESIAN_POINT('Ctrl Pts',(-20.3993237481874,25.9068513714101,-30.0931934999995));
#65808=CARTESIAN_POINT('Ctrl Pts',(-20.3326995878065,25.8120752597787,-30.0990581869377));
#65809=CARTESIAN_POINT('Ctrl Pts',(-20.266143946204,25.7173966194451,-30.1049168424125));
#65810=CARTESIAN_POINT('Ctrl Pts',(-20.2036994047332,25.6196762256278,-30.1107754978873));
#65811=CARTESIAN_POINT('Ctrl Pts',(-20.1456515283854,25.5193083989232,-30.1166341533622));
#65812=CARTESIAN_POINT('Ctrl Pts',(-20.0853362508596,25.4150201165048,-30.1227216530801));
#65813=CARTESIAN_POINT('Ctrl Pts',(-20.02976840905,25.3078737102556,-30.128809152798));
#65814=CARTESIAN_POINT('Ctrl Pts',(-19.9792192324939,25.1983454222809,-30.1348966525159));
#65815=CARTESIAN_POINT('Ctrl Pts',(-19.9306266694158,25.0930566598353,-30.1407485225993));
#65816=CARTESIAN_POINT('Ctrl Pts',(-19.8866716688742,24.9855673889998,-30.1466003926827));
#65817=CARTESIAN_POINT('Ctrl Pts',(-19.8475481253974,24.876325334971,-30.1524522627661));
#65818=CARTESIAN_POINT('Ctrl Pts',(-19.8084305388359,24.7670999140384,-30.1583032418491));
#65819=CARTESIAN_POINT('Ctrl Pts',(-19.7741430860048,24.6561226296204,-30.1641542209321));
#65820=CARTESIAN_POINT('Ctrl Pts',(-19.7448308458809,24.5438594927919,-30.170005200015));
#65821=CARTESIAN_POINT('Ctrl Pts',(-19.7155159703045,24.4315862624271,-30.1758567051573));
#65822=CARTESIAN_POINT('Ctrl Pts',(-19.6911773011056,24.3180273498262,-30.1817082102996));
#65823=CARTESIAN_POINT('Ctrl Pts',(-19.6719093607071,24.2036614756626,-30.1875597154419));
#65824=CARTESIAN_POINT('Ctrl Pts',(-19.6526350218451,24.0892576230818,-30.1934131637417));
#65825=CARTESIAN_POINT('Ctrl Pts',(-19.6384348287113,23.9740466835105,-30.1992666120415));
#65826=CARTESIAN_POINT('Ctrl Pts',(-19.6293516591246,23.8585143481477,-30.2051200603413));
#65827=CARTESIAN_POINT('Ctrl Pts',(-19.6202581600018,23.7428506274324,-30.2109801652829));
#65828=CARTESIAN_POINT('Ctrl Pts',(-19.6162933317269,23.6268651937607,-30.2168402702244));
#65829=CARTESIAN_POINT('Ctrl Pts',(-19.6174479567391,23.5110457056012,-30.222700375166));
#65830=CARTESIAN_POINT('Ctrl Pts',(-19.618603359319,23.3951482202654,-30.2285644265214));
#65831=CARTESIAN_POINT('Ctrl Pts',(-19.6248850577546,23.2794173147327,-30.2344284778769));
#65832=CARTESIAN_POINT('Ctrl Pts',(-19.6362319350756,23.1643357411226,-30.2402925292323));
#65833=CARTESIAN_POINT('Ctrl Pts',(-19.6475955354286,23.0490845602455,-30.2461652230289));
#65834=CARTESIAN_POINT('Ctrl Pts',(-19.6640391549982,22.9344850289054,-30.2520379168255));
#65835=CARTESIAN_POINT('Ctrl Pts',(-19.6854505508007,22.8210100147757,-30.2579106106221));
#65836=CARTESIAN_POINT('Ctrl Pts',(-19.6913126328021,22.7899424541141,-30.2595184559453));
#65837=CARTESIAN_POINT('Ctrl Pts',(-19.6975467976592,22.7589590954733,-30.2611263012686));
#65838=CARTESIAN_POINT('Ctrl Pts',(-19.7041500967817,22.7280694254704,-30.2627341465918));
#65839=CARTESIAN_POINT('Ctrl Pts',(-19.7282671762418,22.6152517850535,-30.2686064435605));
#65840=CARTESIAN_POINT('Ctrl Pts',(-19.7573927830819,22.5033071828822,-30.2744787405292));
#65841=CARTESIAN_POINT('Ctrl Pts',(-19.7914502153492,22.392714564006,-30.2803510374979));
#65842=CARTESIAN_POINT('Ctrl Pts',(-19.8254635118892,22.2822652643807,-30.2862157244361));
#65843=CARTESIAN_POINT('Ctrl Pts',(-19.8643958034048,22.1731648552529,-30.2920804113743));
#65844=CARTESIAN_POINT('Ctrl Pts',(-19.9081193532127,22.0658823251069,-30.2979450983125));
#65845=CARTESIAN_POINT('Ctrl Pts',(-19.9517979360866,21.9587101283272,-30.3038037537873));
#65846=CARTESIAN_POINT('Ctrl Pts',(-20.0002578211049,21.8533524723583,-30.3096624092621));
#65847=CARTESIAN_POINT('Ctrl Pts',(-20.0533216197173,21.7502627548175,-30.315521064737));
#65848=CARTESIAN_POINT('Ctrl Pts',(-20.1084581370416,21.6431462621091,-30.3216085644549));
#65849=CARTESIAN_POINT('Ctrl Pts',(-20.1685654321618,21.5384789296272,-30.3276960641728));
#65850=CARTESIAN_POINT('Ctrl Pts',(-20.2333894456673,21.4367463763798,-30.3337835638907));
#65851=CARTESIAN_POINT('Ctrl Pts',(-20.2957043077447,21.338951598155,-30.3396354339741));
#65852=CARTESIAN_POINT('Ctrl Pts',(-20.3623772936025,21.2438690110315,-30.3454873040575));
#65853=CARTESIAN_POINT('Ctrl Pts',(-20.4331365327328,21.1519037561783,-30.3513391741409));
#65854=CARTESIAN_POINT('Ctrl Pts',(-20.5038849981255,21.0599525038713,-30.3571901532238));
#65855=CARTESIAN_POINT('Ctrl Pts',(-20.5787182277069,20.9711179676324,-30.3630411323068));
#65856=CARTESIAN_POINT('Ctrl Pts',(-20.6573225798779,20.8857741035803,-30.3688921113898));
#65857=CARTESIAN_POINT('Ctrl Pts',(-20.7359339993367,20.8004225662935,-30.374743616532));
#65858=CARTESIAN_POINT('Ctrl Pts',(-20.8183169353355,20.7185626291716,-30.3805951216743));
#65859=CARTESIAN_POINT('Ctrl Pts',(-20.9041197255165,20.6405325843333,-30.3864466268166));
#65860=CARTESIAN_POINT('Ctrl Pts',(-20.9899510089364,20.5624766274156,-30.3923000751164));
#65861=CARTESIAN_POINT('Ctrl Pts',(-21.0792040990572,20.4882533697011,-30.3981535234162));
#65862=CARTESIAN_POINT('Ctrl Pts',(-21.1714935530031,20.4181614217013,-30.4040069717159));
#65863=CARTESIAN_POINT('Ctrl Pts',(-21.2638879600984,20.3479897639365,-30.4098670766575));
#65864=CARTESIAN_POINT('Ctrl Pts',(-21.3593252937146,20.2819590435148,-30.415727181599));
#65865=CARTESIAN_POINT('Ctrl Pts',(-21.4573902961179,20.2203251056234,-30.4215872865405));
#65866=CARTESIAN_POINT('Ctrl Pts',(-21.5555213391625,20.1586496611323,-30.427451337896));
#65867=CARTESIAN_POINT('Ctrl Pts',(-21.656283216053,20.1013770988003,-30.4333153892514));
#65868=CARTESIAN_POINT('Ctrl Pts',(-21.759236743018,20.0487169478806,-30.4391794406068));
#65869=CARTESIAN_POINT('Ctrl Pts',(-21.8623420029303,19.9959791864105,-30.4450521344034));
#65870=CARTESIAN_POINT('Ctrl Pts',(-21.9676449848974,19.947867574541,-30.4509248282));
#65871=CARTESIAN_POINT('Ctrl Pts',(-22.0746871853209,19.9045432853908,-30.4567975219965));
#65872=CARTESIAN_POINT('Ctrl Pts',(-22.103993549201,19.8926818197477,-30.4584053673199));
#65873=CARTESIAN_POINT('Ctrl Pts',(-22.1334301990654,19.8811789084159,-30.4600132126433));
#65874=CARTESIAN_POINT('Ctrl Pts',(-22.1629875598261,19.8700371986155,-30.4616210579668));
#65875=CARTESIAN_POINT('Ctrl Pts',(-22.2709392374352,19.8293445848829,-30.4674933549355));
#65876=CARTESIAN_POINT('Ctrl Pts',(-22.3808637346955,19.7933376434519,-30.4733656519042));
#65877=CARTESIAN_POINT('Ctrl Pts',(-22.4923166464442,19.7622107337859,-30.4792379488729));
#65878=CARTESIAN_POINT('Ctrl Pts',(-22.6036251240706,19.7311241621228,-30.4851026358111));
#65879=CARTESIAN_POINT('Ctrl Pts',(-22.7164576828048,19.7049051559623,-30.4909673227493));
#65880=CARTESIAN_POINT('Ctrl Pts',(-22.8303507076736,19.683699756447,-30.4968320096875));
#65881=CARTESIAN_POINT('Ctrl Pts',(-22.9441266006961,19.6625161653576,-30.5026906651623));
#65882=CARTESIAN_POINT('Ctrl Pts',(-23.0589603865923,19.6463360002162,-30.5085493206371));
#65883=CARTESIAN_POINT('Ctrl Pts',(-23.1743747283084,19.6352551016922,-30.5144079761119));
#65884=CARTESIAN_POINT('Ctrl Pts',(-23.2942972558676,19.623741373512,-30.5204954758298));
#65885=CARTESIAN_POINT('Ctrl Pts',(-23.4148461799605,19.6177335190221,-30.5265829755478));
#65886=CARTESIAN_POINT('Ctrl Pts',(-23.5354756112862,19.6172802914383,-30.5326704752657));
#65887=CARTESIAN_POINT('Ctrl Pts',(-23.6514358236992,19.6168446069929,-30.5385223453491));
#65888=CARTESIAN_POINT('Ctrl Pts',(-23.7674699748903,19.6215415394737,-30.5443742154325));
#65889=CARTESIAN_POINT('Ctrl Pts',(-23.8830902552613,19.6313613556381,-30.5502260855159));
#65890=CARTESIAN_POINT('Ctrl Pts',(-23.9986929313934,19.6411796766461,-30.5560770645988));
#65891=CARTESIAN_POINT('Ctrl Pts',(-24.1138814502137,19.656119295463,-30.5619280436818));
#65892=CARTESIAN_POINT('Ctrl Pts',(-24.2281716595849,19.6761184792846,-30.5677790227648));
#65893=CARTESIAN_POINT('Ctrl Pts',(-24.3424721447459,19.6961194612252,-30.5736305279071));
#65894=CARTESIAN_POINT('Ctrl Pts',(-24.455873752681,19.721180841219,-30.5794820330494));
#65895=CARTESIAN_POINT('Ctrl Pts',(-24.5679017841425,19.7511896210554,-30.5853335381917));
#65896=CARTESIAN_POINT('Ctrl Pts',(-24.6799670176746,19.7812083661544,-30.5911869864915));
#65897=CARTESIAN_POINT('Ctrl Pts',(-24.7906573686438,19.8161776710418,-30.5970404347913));
#65898=CARTESIAN_POINT('Ctrl Pts',(-24.8995132628018,19.8559346677996,-30.602893883091));
#65899=CARTESIAN_POINT('Ctrl Pts',(-25.0084929497488,19.8957368768956,-30.6087539880326));
#65900=CARTESIAN_POINT('Ctrl Pts',(-25.1156336274148,19.9403375033096,-30.6146140929741));
#65901=CARTESIAN_POINT('Ctrl Pts',(-25.220495584542,19.9895254789122,-30.6204741979157));
#65902=CARTESIAN_POINT('Ctrl Pts',(-25.3254281596342,20.0387465795378,-30.6263382492711));
#65903=CARTESIAN_POINT('Ctrl Pts',(-25.428078593316,20.092560989277,-30.6322023006266));
#65904=CARTESIAN_POINT('Ctrl Pts',(-25.5280332076643,20.1507124748984,-30.638066351982));
#65905=CARTESIAN_POINT('Ctrl Pts',(-25.6281351351613,20.2089496642014,-30.6439390457786));
#65906=CARTESIAN_POINT('Ctrl Pts',(-25.7255329673192,20.2715364639187,-30.6498117395752));
#65907=CARTESIAN_POINT('Ctrl Pts',(-25.8198432658568,20.3381742481832,-30.6556844333718));
#65908=CARTESIAN_POINT('Ctrl Pts',(-25.8456638479769,20.3564185588002,-30.657292278695));
#65909=CARTESIAN_POINT('Ctrl Pts',(-25.8712531974368,20.3749662950071,-30.6589001240183));
#65910=CARTESIAN_POINT('Ctrl Pts',(-25.8966039113448,20.3938108320565,-30.6605079693416));
#65911=CARTESIAN_POINT('Ctrl Pts',(-25.9882908702291,20.4619666362644,-30.6663231289692));
#65912=CARTESIAN_POINT('Ctrl Pts',(-26.0771739154361,20.534245915364,-30.6721382885967));
#65913=CARTESIAN_POINT('Ctrl Pts',(-26.1628535832494,20.610387782184,-30.6779534482243));
#65914=CARTESIAN_POINT('Ctrl Pts',(-26.2484218402025,20.6864306403232,-30.683761046292));
#65915=CARTESIAN_POINT('Ctrl Pts',(-26.3307946872854,20.7663258245341,-30.6895686443597));
#65916=CARTESIAN_POINT('Ctrl Pts',(-26.4096025433909,20.8497698876822,-30.6953762424275));
#65917=CARTESIAN_POINT('Ctrl Pts',(-26.4883300325188,20.9331288559236,-30.7011779180006));
#65918=CARTESIAN_POINT('Ctrl Pts',(-26.5634994709374,21.0200292023037,-30.7069795935737));
#65919=CARTESIAN_POINT('Ctrl Pts',(-26.6347758320368,21.1101285574577,-30.7127812691468));
#65920=CARTESIAN_POINT('Ctrl Pts',(-26.7060007161387,21.2001628413286,-30.7185787546513));
#65921=CARTESIAN_POINT('Ctrl Pts',(-26.7733378530381,21.2933912095816,-30.7243762401559));
#65922=CARTESIAN_POINT('Ctrl Pts',(-26.8364909749819,21.3894365067031,-30.7301737256604));
#65923=CARTESIAN_POINT('Ctrl Pts',(-26.8996204763624,21.485445880913,-30.7359690427865));
#65924=CARTESIAN_POINT('Ctrl Pts',(-26.958568840997,21.5842697379139,-30.7417643599125));
#65925=CARTESIAN_POINT('Ctrl Pts',(-27.0130822241071,21.6855006658033,-30.7475596770385));
#65926=CARTESIAN_POINT('Ctrl Pts',(-27.0675890491965,21.7867194154993,-30.7533542969815));
#65927=CARTESIAN_POINT('Ctrl Pts',(-27.1176617535317,21.8903442885566,-30.7591489169244));
#65928=CARTESIAN_POINT('Ctrl Pts',(-27.1630921076474,21.9959426531866,-30.7649435368673));
#65929=CARTESIAN_POINT('Ctrl Pts',(-27.2085285233355,22.1015551073422,-30.7707389299609));
#65930=CARTESIAN_POINT('Ctrl Pts',(-27.2493211918264,22.2091411881512,-30.7765343230545));
#65931=CARTESIAN_POINT('Ctrl Pts',(-27.2853100775913,22.3182484209717,-30.7823297161481));
#65932=CARTESIAN_POINT('Ctrl Pts',(-27.3213335965694,22.4274606510428,-30.7881306863269));
#65933=CARTESIAN_POINT('Ctrl Pts',(-27.3525439703304,22.5381965543137,-30.7939316565058));
#65934=CARTESIAN_POINT('Ctrl Pts',(-27.3788311109258,22.6499886466868,-30.7997326266846));
#65935=CARTESIAN_POINT('Ctrl Pts',(-27.4051318832004,22.7618387109008,-30.805536605063));
#65936=CARTESIAN_POINT('Ctrl Pts',(-27.4265042609705,22.8747456401159,-30.8113405834414));
#65937=CARTESIAN_POINT('Ctrl Pts',(-27.4428896676765,22.9882337352369,-30.8171445618198));
#65938=CARTESIAN_POINT('Ctrl Pts',(-27.459299555236,23.1018913888848,-30.8229572117159));
#65939=CARTESIAN_POINT('Ctrl Pts',(-27.4707075521564,23.2161315225773,-30.828769861612));
#65940=CARTESIAN_POINT('Ctrl Pts',(-27.4771071121635,23.3304751355696,-30.8345825115081));
#65941=CARTESIAN_POINT('Ctrl Pts',(-27.481237209735,23.4042693148278,-30.8383338336604));
#65942=CARTESIAN_POINT('Ctrl Pts',(-27.4832823320317,23.478106587533,-30.8420851558128));
#65943=CARTESIAN_POINT('Ctrl Pts',(-27.4832522035277,23.5518591921931,-30.8458364779651));
#65944=CARTESIAN_POINT('',(-27.4838863721737,23.5466573194615,-32.0958364779651));
#65945=CARTESIAN_POINT('Ctrl Pts',(-27.4889592910419,23.5518615235821,-30.8458364779651));
#65946=CARTESIAN_POINT('Ctrl Pts',(-27.4894190108028,23.6408453350039,-30.8503559455489));
#65947=CARTESIAN_POINT('Ctrl Pts',(-27.4866659078226,23.7298001893193,-30.8548754131327));
#65948=CARTESIAN_POINT('Ctrl Pts',(-27.3917678005741,25.1200922643632,-30.9256905178415));
#65949=CARTESIAN_POINT('Ctrl Pts',(-25.7924728177291,27.6261817534798,-31.0582817920914));
#65950=CARTESIAN_POINT('Ctrl Pts',(-21.3331200095261,27.6398826141405,-31.2571687034663));
#65951=CARTESIAN_POINT('Ctrl Pts',(-18.9111240073572,23.8955601724853,-31.4560556148412));
#65952=CARTESIAN_POINT('Ctrl Pts',(-20.7520937858179,19.8339292862019,-31.6549425262161));
#65953=CARTESIAN_POINT('Ctrl Pts',(-25.1643342070015,19.1872843702764,-31.853829437591));
#65954=CARTESIAN_POINT('Ctrl Pts',(-27.3287038009197,21.6719949499706,-32.000794088174));
#65955=CARTESIAN_POINT('Ctrl Pts',(-27.4865274055665,23.262709423076,-32.081463101632));
#65956=CARTESIAN_POINT('Ctrl Pts',(-27.4838863721737,23.5466573194615,-32.0958364779651));
#65957=CARTESIAN_POINT('',(-27.4767290463135,23.5502914556789,-33.3458364779651));
#65958=CARTESIAN_POINT('Ctrl Pts',(-27.4838863721737,23.5466573194615,-32.0958364779651));
#65959=CARTESIAN_POINT('Ctrl Pts',(-27.4743459259068,24.5723882532228,-32.147758738757));
#65960=CARTESIAN_POINT('Ctrl Pts',(-26.5386620802302,26.923215037617,-32.2659766366737));
#65961=CARTESIAN_POINT('Ctrl Pts',(-22.5719187031782,28.098176646286,-32.4504901717156));
#65962=CARTESIAN_POINT('Ctrl Pts',(-19.1951767590657,25.1855096511627,-32.6493770830904));
#65963=CARTESIAN_POINT('Ctrl Pts',(-19.8203802004651,20.7701800101868,-32.8482639944654));
#65964=CARTESIAN_POINT('Ctrl Pts',(-23.8730200732411,18.9095013051974,-33.0471509058403));
#65965=CARTESIAN_POINT('Ctrl Pts',(-27.0052926844262,20.9140808275611,-33.2130084003402));
#65966=CARTESIAN_POINT('Ctrl Pts',(-27.4766710115324,22.8900833516303,-33.3125702577151));
#65967=CARTESIAN_POINT('Ctrl Pts',(-27.4767290463135,23.5502914556789,-33.3458364779651));
#65968=CARTESIAN_POINT('',(-27.4840297199183,23.553834420186,-34.5958364779651));
#65969=CARTESIAN_POINT('Ctrl Pts',(-27.4767290463135,23.5502914556789,-33.3458364779651));
#65970=CARTESIAN_POINT('Ctrl Pts',(-27.4767866679778,24.2057999122759,-33.3788658948401));
#65971=CARTESIAN_POINT('Ctrl Pts',(-27.0102223100593,26.1769478082497,-33.4781909488402));
#65972=CARTESIAN_POINT('Ctrl Pts',(-23.889589688675,28.1898215985353,-33.6438116399649));
#65973=CARTESIAN_POINT('Ctrl Pts',(-19.8303313507955,26.3436263412674,-33.8426985513399));
#65974=CARTESIAN_POINT('Ctrl Pts',(-19.1893651808564,21.9305573920422,-34.0415854627147));
#65975=CARTESIAN_POINT('Ctrl Pts',(-22.5556847440637,19.0058509486566,-34.2404723740897));
#65976=CARTESIAN_POINT('Ctrl Pts',(-26.531694747342,20.168129958384,-34.4252227125063));
#65977=CARTESIAN_POINT('Ctrl Pts',(-27.4744466997929,22.5235216847793,-34.5436774137982));
#65978=CARTESIAN_POINT('Ctrl Pts',(-27.4840297199183,23.553834420186,-34.5958364779651));
#65979=CARTESIAN_POINT('',(-27.4847809928552,23.5485683047834,-35.8458364779651));
#65980=CARTESIAN_POINT('Ctrl Pts',(-27.4840297199183,23.553834420186,-34.5958364779651));
#65981=CARTESIAN_POINT('Ctrl Pts',(-27.4866269878204,23.8330781410309,-34.6099730509232));
#65982=CARTESIAN_POINT('Ctrl Pts',(-27.3319136679028,25.4190216835505,-34.6904052610063));
#65983=CARTESIAN_POINT('Ctrl Pts',(-25.1799036529807,27.9074291467727,-34.8371331082142));
#65984=CARTESIAN_POINT('Ctrl Pts',(-20.765382256512,27.2765440370006,-35.0360200195892));
#65985=CARTESIAN_POINT('Ctrl Pts',(-18.9099205248741,23.2215129712688,-35.2349069309641));
#65986=CARTESIAN_POINT('Ctrl Pts',(-21.3185304722301,19.468565689051,-35.433793842339));
#65987=CARTESIAN_POINT('Ctrl Pts',(-25.7779037734052,19.4663425452466,-35.6326807537138));
#65988=CARTESIAN_POINT('Ctrl Pts',(-27.4438276006778,22.0563973201223,-35.7700282989226));
#65989=CARTESIAN_POINT('Ctrl Pts',(-27.4893831213271,23.4549152959221,-35.8410802070063));
#65990=CARTESIAN_POINT('Ctrl Pts',(-27.48887967105,23.54856655029,-35.8458364779651));
#65991=CARTESIAN_POINT('',(-27.4823337739288,23.5474881844497,-37.0958364389384));
#65992=CARTESIAN_POINT('Ctrl Pts',(-27.4832521713565,23.5485689592156,-35.8458364779651));
#65993=CARTESIAN_POINT('Ctrl Pts',(-27.4833010804302,23.6628256197236,-35.8516475539864));
#65994=CARTESIAN_POINT('Ctrl Pts',(-27.4783669067839,23.7772857692739,-35.8574586300076));
#65995=CARTESIAN_POINT('Ctrl Pts',(-27.4684227067072,23.8914731049878,-35.8632697060289));
#65996=CARTESIAN_POINT('Ctrl Pts',(-27.4584907720493,24.0055195992575,-35.8690736145273));
#65997=CARTESIAN_POINT('Ctrl Pts',(-27.4435611311356,24.1192935314233,-35.8748775230257));
#65998=CARTESIAN_POINT('Ctrl Pts',(-27.4236588403682,24.2323174610992,-35.8806814315241));
#65999=CARTESIAN_POINT('Ctrl Pts',(-27.4037755068557,24.3452337336485,-35.8864798117056));
#66000=CARTESIAN_POINT('Ctrl Pts',(-27.3789290140938,24.4574010102805,-35.892278191887));
#66001=CARTESIAN_POINT('Ctrl Pts',(-27.3491962524981,24.5683466364628,-35.8980765720684));
#66002=CARTESIAN_POINT('Ctrl Pts',(-27.3194819609759,24.6792233429163,-35.90387135028));
#66003=CARTESIAN_POINT('Ctrl Pts',(-27.2848875439982,24.7888795006092,-35.9096661284917));
#66004=CARTESIAN_POINT('Ctrl Pts',(-27.245540894086,24.8968530362135,-35.9154609067034));
#66005=CARTESIAN_POINT('Ctrl Pts',(-27.2062064694983,25.0047930235612,-35.9212538844303));
#66006=CARTESIAN_POINT('Ctrl Pts',(-27.1621228906993,25.1110510310645,-35.9270468621571));
#66007=CARTESIAN_POINT('Ctrl Pts',(-27.1134675588383,25.2151812599989,-35.932839839884));
#66008=CARTESIAN_POINT('Ctrl Pts',(-27.0648149810358,25.3193055948056,-35.9386324897085));
#66009=CARTESIAN_POINT('Ctrl Pts',(-27.0115913437918,25.4213020077496,-35.944425139533));
#66010=CARTESIAN_POINT('Ctrl Pts',(-26.9540213827635,25.5207465328245,-35.9502177893575));
#66011=CARTESIAN_POINT('Ctrl Pts',(-26.8964400508042,25.620210699685,-35.9560115833173));
#66012=CARTESIAN_POINT('Ctrl Pts',(-26.8345109012256,25.7171216116196,-35.961805377277));
#66013=CARTESIAN_POINT('Ctrl Pts',(-26.7685031915193,25.8110823993612,-35.9675991712368));
#66014=CARTESIAN_POINT('Ctrl Pts',(-26.7024260487529,25.9051420238152,-35.9733990596489));
#66015=CARTESIAN_POINT('Ctrl Pts',(-26.6322620242447,25.9962449826675,-35.9791989480611));
#66016=CARTESIAN_POINT('Ctrl Pts',(-26.5583220564273,26.0840257524802,-35.9849988364732));
#66017=CARTESIAN_POINT('Ctrl Pts',(-26.4843396080464,26.1718569547812,-35.9908020570822));
#66018=CARTESIAN_POINT('Ctrl Pts',(-26.4065771839923,26.2563618583141,-35.9966052776912));
#66019=CARTESIAN_POINT('Ctrl Pts',(-26.3253828185495,26.3372116076367,-36.0024084983002));
#66020=CARTESIAN_POINT('Ctrl Pts',(-26.2440619203749,26.4181873526437,-36.0082207626077));
#66021=CARTESIAN_POINT('Ctrl Pts',(-26.1592987145201,26.4954962868289,-36.0140330269151));
#66022=CARTESIAN_POINT('Ctrl Pts',(-26.0714746767591,26.5688495394504,-36.0198452912225));
#66023=CARTESIAN_POINT('Ctrl Pts',(-26.0180388028701,26.6134807731804,-36.0233817196362));
#66024=CARTESIAN_POINT('Ctrl Pts',(-25.9634703998983,26.6566484310142,-36.0269181480499));
#66025=CARTESIAN_POINT('Ctrl Pts',(-25.9078602994194,26.6982955132244,-36.0304545764636));
#66026=CARTESIAN_POINT('Ctrl Pts',(-25.81551882201,26.7674511714226,-36.0363268734323));
#66027=CARTESIAN_POINT('Ctrl Pts',(-25.7199772556527,26.8326562634563,-36.042199170401));
#66028=CARTESIAN_POINT('Ctrl Pts',(-25.6216082656292,26.8936003184933,-36.0480714673697));
#66029=CARTESIAN_POINT('Ctrl Pts',(-25.5233667540044,26.9544653948751,-36.0539361543079));
#66030=CARTESIAN_POINT('Ctrl Pts',(-25.422305453489,27.0110801997646,-36.0598008412462));
#66031=CARTESIAN_POINT('Ctrl Pts',(-25.318828939574,27.0631753161418,-36.0656655281844));
#66032=CARTESIAN_POINT('Ctrl Pts',(-25.2154588447757,27.115216855953,-36.0715241836592));
#66033=CARTESIAN_POINT('Ctrl Pts',(-25.1096788441844,27.1627477680231,-36.077382839134));
#66034=CARTESIAN_POINT('Ctrl Pts',(-25.0019206773712,27.2055430255984,-36.0832414946088));
#66035=CARTESIAN_POINT('Ctrl Pts',(-24.8899533816501,27.2500099036282,-36.0893289943267));
#66036=CARTESIAN_POINT('Ctrl Pts',(-24.7758506179667,27.2893633880399,-36.0954164940446));
#66037=CARTESIAN_POINT('Ctrl Pts',(-24.6601230822019,27.323404577546,-36.1015039937625));
#66038=CARTESIAN_POINT('Ctrl Pts',(-24.5488750270478,27.3561281303518,-36.107355863846));
#66039=CARTESIAN_POINT('Ctrl Pts',(-24.436126075118,27.3839428612702,-36.1132077339294));
#66040=CARTESIAN_POINT('Ctrl Pts',(-24.3223474355458,27.4067222203403,-36.1190596040128));
#66041=CARTESIAN_POINT('Ctrl Pts',(-24.2085861198059,27.429498111046,-36.1249105830957));
#66042=CARTESIAN_POINT('Ctrl Pts',(-24.0937958333789,27.4472400731813,-36.1307615621787));
#66043=CARTESIAN_POINT('Ctrl Pts',(-23.9784587591846,27.4598725166465,-36.1366125412617));
#66044=CARTESIAN_POINT('Ctrl Pts',(-23.8631113150775,27.47250609589,-36.142464046404));
#66045=CARTESIAN_POINT('Ctrl Pts',(-23.7472173964247,27.4800291982189,-36.1483155515463));
#66046=CARTESIAN_POINT('Ctrl Pts',(-23.6312643894131,27.4824181028406,-36.1541670566886));
#66047=CARTESIAN_POINT('Ctrl Pts',(-23.5152728769322,27.4848078007655,-36.1600205049883));
#66048=CARTESIAN_POINT('Ctrl Pts',(-23.399222650152,27.4820599022765,-36.1658739532881));
#66049=CARTESIAN_POINT('Ctrl Pts',(-23.283600462147,27.4742027956255,-36.1717274015878));
#66050=CARTESIAN_POINT('Ctrl Pts',(-23.1678467866071,27.466336753738,-36.1775875065294));
#66051=CARTESIAN_POINT('Ctrl Pts',(-23.052522534103,27.4533499345903,-36.1834476114709));
#66052=CARTESIAN_POINT('Ctrl Pts',(-22.9381088090778,27.4353225520235,-36.1893077164124));
#66053=CARTESIAN_POINT('Ctrl Pts',(-22.8236180335695,27.4172830291428,-36.1951717677679));
#66054=CARTESIAN_POINT('Ctrl Pts',(-22.7100394106186,27.3941962658534,-36.2010358191233));
#66055=CARTESIAN_POINT('Ctrl Pts',(-22.597841624427,27.3661931056181,-36.2068998704788));
#66056=CARTESIAN_POINT('Ctrl Pts',(-22.4854784810952,27.3381486743145,-36.2127725642754));
#66057=CARTESIAN_POINT('Ctrl Pts',(-22.3745006309178,27.3051735021705,-36.2186452580719));
#66058=CARTESIAN_POINT('Ctrl Pts',(-22.2653595256975,27.2674475713902,-36.2245179518685));
#66059=CARTESIAN_POINT('Ctrl Pts',(-22.2354785167956,27.2571188426202,-36.2261257971919));
#66060=CARTESIAN_POINT('Ctrl Pts',(-22.20573505551,27.2464342820289,-36.2277336425152));
#66061=CARTESIAN_POINT('Ctrl Pts',(-22.1761380972322,27.2353981897386,-36.2293414878386));
#66062=CARTESIAN_POINT('Ctrl Pts',(-22.0680417985066,27.1950913204384,-36.2352137848073));
#66063=CARTESIAN_POINT('Ctrl Pts',(-21.9615393936409,27.1499567141263,-36.241086081776));
#66064=CARTESIAN_POINT('Ctrl Pts',(-21.8570935283387,27.1001400777097,-36.2469583787447));
#66065=CARTESIAN_POINT('Ctrl Pts',(-21.752783016583,27.0503879996976,-36.2528230656829));
#66066=CARTESIAN_POINT('Ctrl Pts',(-21.6505241141111,26.9959661340572,-36.2586877526211));
#66067=CARTESIAN_POINT('Ctrl Pts',(-21.5507621761864,26.9370692256166,-36.2645524395593));
#66068=CARTESIAN_POINT('Ctrl Pts',(-21.4511028371693,26.8782328889591,-36.2704110950341));
#66069=CARTESIAN_POINT('Ctrl Pts',(-21.3539357087071,26.8149308726108,-36.2762697505089));
#66070=CARTESIAN_POINT('Ctrl Pts',(-21.2596834831239,26.7474047698167,-36.2821284059838));
#66071=CARTESIAN_POINT('Ctrl Pts',(-21.1617496825934,26.6772410379715,-36.2882159057017));
#66072=CARTESIAN_POINT('Ctrl Pts',(-21.0669635549451,26.6025166950774,-36.2943034054196));
#66073=CARTESIAN_POINT('Ctrl Pts',(-20.9757684919428,26.5235538835698,-36.3003909051375));
#66074=CARTESIAN_POINT('Ctrl Pts',(-20.888103327973,26.4476474957629,-36.3062427752209));
#66075=CARTESIAN_POINT('Ctrl Pts',(-20.8037567398837,26.3678249519861,-36.3120946453042));
#66076=CARTESIAN_POINT('Ctrl Pts',(-20.7230899047927,26.284414282771,-36.3179465153876));
#66077=CARTESIAN_POINT('Ctrl Pts',(-20.6424353519607,26.2010163135886,-36.3237974944706));
#66078=CARTESIAN_POINT('Ctrl Pts',(-20.5654597254178,26.114031602307,-36.3296484735536));
#66079=CARTESIAN_POINT('Ctrl Pts',(-20.4924872606926,26.0238249578536,-36.3354994526366));
#66080=CARTESIAN_POINT('Ctrl Pts',(-20.4195082350406,25.933610202955,-36.3413509577788));
#66081=CARTESIAN_POINT('Ctrl Pts',(-20.350533346703,25.8401732604312,-36.3472024629211));
#66082=CARTESIAN_POINT('Ctrl Pts',(-20.2858460052765,25.7439113543651,-36.3530539680634));
#66083=CARTESIAN_POINT('Ctrl Pts',(-20.2211371825919,25.647617481815,-36.3589074163632));
#66084=CARTESIAN_POINT('Ctrl Pts',(-20.1607189684023,25.54849712328,-36.364760864663));
#66085=CARTESIAN_POINT('Ctrl Pts',(-20.1048305898669,25.4469751373419,-36.3706143129627));
#66086=CARTESIAN_POINT('Ctrl Pts',(-20.0488786541094,25.3453376988611,-36.3764744179043));
#66087=CARTESIAN_POINT('Ctrl Pts',(-19.9974670355339,25.2412935439909,-36.3823345228458));
#66088=CARTESIAN_POINT('Ctrl Pts',(-19.950788306237,25.1352907929529,-36.3881946277874));
#66089=CARTESIAN_POINT('Ctrl Pts',(-19.9040781417375,25.0292166556966,-36.3940586791428));
#66090=CARTESIAN_POINT('Ctrl Pts',(-19.8621073624037,24.9211816802824,-36.3999227304983));
#66091=CARTESIAN_POINT('Ctrl Pts',(-19.8250192311154,24.8116509050318,-36.4057867818537));
#66092=CARTESIAN_POINT('Ctrl Pts',(-19.787876439325,24.7019587032828,-36.4116594756503));
#66093=CARTESIAN_POINT('Ctrl Pts',(-19.7556307722095,24.5907666974543,-36.4175321694469));
#66094=CARTESIAN_POINT('Ctrl Pts',(-19.7283748365586,24.4785519895337,-36.4234048632434));
#66095=CARTESIAN_POINT('Ctrl Pts',(-19.7209126173136,24.4478294796281,-36.4250127085667));
#66096=CARTESIAN_POINT('Ctrl Pts',(-19.7138241156677,24.4170303486559,-36.4266205538901));
#66097=CARTESIAN_POINT('Ctrl Pts',(-19.7071105546248,24.3861644553363,-36.4282283992134));
#66098=CARTESIAN_POINT('Ctrl Pts',(-19.682590768057,24.2734336539658,-36.4341006961821));
#66099=CARTESIAN_POINT('Ctrl Pts',(-19.6629942048396,24.1594342257253,-36.4399729931508));
#66100=CARTESIAN_POINT('Ctrl Pts',(-19.6484483589224,24.0446341629677,-36.4458452901195));
#66101=CARTESIAN_POINT('Ctrl Pts',(-19.6339213632663,23.9299828719743,-36.4517099770577));
#66102=CARTESIAN_POINT('Ctrl Pts',(-19.6244321200844,23.8145334161144,-36.4575746639959));
#66103=CARTESIAN_POINT('Ctrl Pts',(-19.6200575206853,23.6987657480786,-36.4634393509341));
#66104=CARTESIAN_POINT('Ctrl Pts',(-19.6156874202879,23.583117139842,-36.4692980064089));
#66105=CARTESIAN_POINT('Ctrl Pts',(-19.6164215165977,23.4671513809737,-36.4751566618838));
#66106=CARTESIAN_POINT('Ctrl Pts',(-19.6222850362848,23.3513546810087,-36.4810153173586));
#66107=CARTESIAN_POINT('Ctrl Pts',(-19.6283775902154,23.2310348599508,-36.4871028170765));
#66108=CARTESIAN_POINT('Ctrl Pts',(-19.6400085133725,23.1108980252912,-36.4931903167944));
#66109=CARTESIAN_POINT('Ctrl Pts',(-19.6571464539655,22.991491341603,-36.4992778165123));
#66110=CARTESIAN_POINT('Ctrl Pts',(-19.6736210340879,22.8767065477774,-36.5051296865957));
#66111=CARTESIAN_POINT('Ctrl Pts',(-19.6951841728816,22.7625968792008,-36.5109815566791));
#66112=CARTESIAN_POINT('Ctrl Pts',(-19.7217551243006,22.6496435146504,-36.5168334267625));
#66113=CARTESIAN_POINT('Ctrl Pts',(-19.7483220300506,22.5367073482771,-36.5226844058455));
#66114=CARTESIAN_POINT('Ctrl Pts',(-19.7798951377277,22.4249275381594,-36.5285353849285));
#66115=CARTESIAN_POINT('Ctrl Pts',(-19.8163427905093,22.3147740637781,-36.5343863640114));
#66116=CARTESIAN_POINT('Ctrl Pts',(-19.8527937202857,22.204610685539,-36.5402378691537));
#66117=CARTESIAN_POINT('Ctrl Pts',(-19.8941199365396,22.0960743261952,-36.546089374296));
#66118=CARTESIAN_POINT('Ctrl Pts',(-19.9401404428872,21.9896181394519,-36.5519408794383));
#66119=CARTESIAN_POINT('Ctrl Pts',(-19.9861762316429,21.883126600927,-36.5577943277381));
#66120=CARTESIAN_POINT('Ctrl Pts',(-20.0369092462645,21.7787169878198,-36.5636477760379));
#66121=CARTESIAN_POINT('Ctrl Pts',(-20.0921113585199,21.6768202200276,-36.5695012243376));
#66122=CARTESIAN_POINT('Ctrl Pts',(-20.1473762475639,21.5748075734836,-36.5753613292791));
#66123=CARTESIAN_POINT('Ctrl Pts',(-20.2071201814014,21.4753138397271,-36.5812214342207));
#66124=CARTESIAN_POINT('Ctrl Pts',(-20.2710702423531,21.3787432608708,-36.5870815391622));
#66125=CARTESIAN_POINT('Ctrl Pts',(-20.3350633696686,21.2821076477736,-36.5929455905177));
#66126=CARTESIAN_POINT('Ctrl Pts',(-20.4032680216245,21.1883994427848,-36.5988096418731));
#66127=CARTESIAN_POINT('Ctrl Pts',(-20.4753703933385,21.0979905482959,-36.6046736932286));
#66128=CARTESIAN_POINT('Ctrl Pts',(-20.5475790295552,21.0074484091439,-36.6105463870251));
#66129=CARTESIAN_POINT('Ctrl Pts',(-20.6236965795987,20.92021559546,-36.6164190808217));
#66130=CARTESIAN_POINT('Ctrl Pts',(-20.7033717074578,20.8366279127399,-36.6222917746183));
#66131=CARTESIAN_POINT('Ctrl Pts',(-20.7251854246639,20.8137430034618,-36.6238996199416));
#66132=CARTESIAN_POINT('Ctrl Pts',(-20.7472656146644,20.7911310921355,-36.625507465265));
#66133=CARTESIAN_POINT('Ctrl Pts',(-20.7696046442387,20.7687985367503,-36.6271153105884));
#66134=CARTESIAN_POINT('Ctrl Pts',(-20.8511929747496,20.6872338517731,-36.6329876075571));
#66135=CARTESIAN_POINT('Ctrl Pts',(-20.9365098332629,20.6091254105994,-36.6388599045258));
#66136=CARTESIAN_POINT('Ctrl Pts',(-21.0252304058443,20.5348334457348,-36.6447322014945));
#66137=CARTESIAN_POINT('Ctrl Pts',(-21.1138360036096,20.4606377573565,-36.6505968884327));
#66138=CARTESIAN_POINT('Ctrl Pts',(-21.2058362296468,20.3902489727126,-36.6564615753709));
#66139=CARTESIAN_POINT('Ctrl Pts',(-21.3008688547163,20.3239912165269,-36.6623262623091));
#66140=CARTESIAN_POINT('Ctrl Pts',(-21.3958037446802,20.2578016022955,-36.6681849177839));
#66141=CARTESIAN_POINT('Ctrl Pts',(-21.4937644934943,20.1957348010321,-36.6740435732588));
#66142=CARTESIAN_POINT('Ctrl Pts',(-21.5943556810036,20.1380748532228,-36.6799022287336));
#66143=CARTESIAN_POINT('Ctrl Pts',(-21.6988760488965,20.0781626570659,-36.6859897284515));
#66144=CARTESIAN_POINT('Ctrl Pts',(-21.8062361906173,20.0230088957691,-36.6920772281694));
#66145=CARTESIAN_POINT('Ctrl Pts',(-21.9159588204585,19.9728829581926,-36.6981647278873));
#66146=CARTESIAN_POINT('Ctrl Pts',(-22.0214344023548,19.9246972517285,-36.7040165979707));
#66147=CARTESIAN_POINT('Ctrl Pts',(-22.1290925717329,19.8811575688695,-36.7098684680541));
#66148=CARTESIAN_POINT('Ctrl Pts',(-22.2384848581532,19.8424560741398,-36.7157203381375));
#66149=CARTESIAN_POINT('Ctrl Pts',(-22.3478604886033,19.8037604720645,-36.7215713172205));
#66150=CARTESIAN_POINT('Ctrl Pts',(-22.4589693215036,19.7699017312436,-36.7274222963034));
#66151=CARTESIAN_POINT('Ctrl Pts',(-22.5713447891374,19.741023130416,-36.7332732753864));
#66152=CARTESIAN_POINT('Ctrl Pts',(-22.6837303604072,19.7121419331243,-36.7391247805287));
#66153=CARTESIAN_POINT('Ctrl Pts',(-22.7973823924009,19.688241868832,-36.744976285671));
#66154=CARTESIAN_POINT('Ctrl Pts',(-22.911821803085,19.6694156110329,-36.7508277908133));
#66155=CARTESIAN_POINT('Ctrl Pts',(-23.0262992166063,19.6505831014434,-36.7566812391131));
#66156=CARTESIAN_POINT('Ctrl Pts',(-23.1415641210529,19.6368278157336,-36.7625346874129));
#66157=CARTESIAN_POINT('Ctrl Pts',(-23.2571306633043,19.6281907562664,-36.7683881357127));
#66158=CARTESIAN_POINT('Ctrl Pts',(-23.3728286298086,19.6195438745872,-36.7742482406543));
#66159=CARTESIAN_POINT('Ctrl Pts',(-23.4888285063129,19.6160268675892,-36.7801083455958));
#66160=CARTESIAN_POINT('Ctrl Pts',(-23.6046426735698,19.6176286350488,-36.7859684505373));
#66161=CARTESIAN_POINT('Ctrl Pts',(-23.7205348344199,19.6192314811984,-36.7918325018928));
#66162=CARTESIAN_POINT('Ctrl Pts',(-23.836240625319,19.6259599418744,-36.7976965532482));
#66163=CARTESIAN_POINT('Ctrl Pts',(-23.9512775337031,19.6377510367726,-36.8035606046037));
#66164=CARTESIAN_POINT('Ctrl Pts',(-24.0664839835267,19.6495595093909,-36.8094332984003));
#66165=CARTESIAN_POINT('Ctrl Pts',(-24.1810191759434,19.6664454475042,-36.8153059921968));
#66166=CARTESIAN_POINT('Ctrl Pts',(-24.294410680147,19.6882947833376,-36.8211786859934));
#66167=CARTESIAN_POINT('Ctrl Pts',(-24.3254553771884,19.6942767659938,-36.8227865313166));
#66168=CARTESIAN_POINT('Ctrl Pts',(-24.3564144363144,19.7006305036489,-36.8243943766399));
#66169=CARTESIAN_POINT('Ctrl Pts',(-24.3872783823627,19.7073530111092,-36.8260022219632));
#66170=CARTESIAN_POINT('Ctrl Pts',(-24.5000020717623,19.7319054724746,-36.8318745189319));
#66171=CARTESIAN_POINT('Ctrl Pts',(-24.611833392709,19.7614630533028,-36.8377468159006));
#66172=CARTESIAN_POINT('Ctrl Pts',(-24.7222936998507,19.7959472031219,-36.8436191128693));
#66173=CARTESIAN_POINT('Ctrl Pts',(-24.8326108592068,19.8303866642215,-36.8494837998075));
#66174=CARTESIAN_POINT('Ctrl Pts',(-24.9415601470675,19.8697398758966,-36.8553484867457));
#66175=CARTESIAN_POINT('Ctrl Pts',(-25.0486730716044,19.9138772917643,-36.8612131736839));
#66176=CARTESIAN_POINT('Ctrl Pts',(-25.1556758372039,19.9579693150629,-36.8670718291587));
#66177=CARTESIAN_POINT('Ctrl Pts',(-25.2608456160637,20.0068355993684,-36.8729304846335));
#66178=CARTESIAN_POINT('Ctrl Pts',(-25.3637296988003,20.0602970069941,-36.8787891401083));
#66179=CARTESIAN_POINT('Ctrl Pts',(-25.4706325244276,20.1158466642898,-36.8848766398262));
#66180=CARTESIAN_POINT('Ctrl Pts',(-25.5750670171097,20.1763576067197,-36.8909641395441));
#66181=CARTESIAN_POINT('Ctrl Pts',(-25.6765485423198,20.2415739019089,-36.897051639262));
#66182=CARTESIAN_POINT('Ctrl Pts',(-25.7741020090817,20.3042658615726,-36.9029035093454));
#66183=CARTESIAN_POINT('Ctrl Pts',(-25.868926479293,20.3713054414222,-36.9087553794288));
#66184=CARTESIAN_POINT('Ctrl Pts',(-25.9606178644304,20.4424192088239,-36.9146072495122));
#66185=CARTESIAN_POINT('Ctrl Pts',(-26.0522952887209,20.5135221485079,-36.9204582285952));
#66186=CARTESIAN_POINT('Ctrl Pts',(-26.140840249884,20.5886977890504,-36.9263092076781));
#66187=CARTESIAN_POINT('Ctrl Pts',(-26.2258800054825,20.6676310474356,-36.9321601867611));
#66188=CARTESIAN_POINT('Ctrl Pts',(-26.3109274069734,20.7465714026803,-36.9380116919034));
#66189=CARTESIAN_POINT('Ctrl Pts',(-26.3924686734077,20.8292697661325,-36.9438631970457));
#66190=CARTESIAN_POINT('Ctrl Pts',(-26.4701668728711,20.9153731719911,-36.9497147021879));
#66191=CARTESIAN_POINT('Ctrl Pts',(-26.5478908742153,21.0015051709165,-36.9555681504877));
#66192=CARTESIAN_POINT('Ctrl Pts',(-26.6217689941519,21.0910441539158,-36.9614215987875));
#66193=CARTESIAN_POINT('Ctrl Pts',(-26.6915041124965,21.1836035281224,-36.9672750470873));
#66194=CARTESIAN_POINT('Ctrl Pts',(-26.7613185348132,21.2762681624363,-36.9731351520288));
#66195=CARTESIAN_POINT('Ctrl Pts',(-26.8269803026443,21.3719597134348,-36.9789952569703));
#66196=CARTESIAN_POINT('Ctrl Pts',(-26.8882351759192,21.4702619387221,-36.9848553619119));
#66197=CARTESIAN_POINT('Ctrl Pts',(-26.9495313005174,21.5686303644055,-36.9907194132673));
#66198=CARTESIAN_POINT('Ctrl Pts',(-27.0064144187566,21.6696126058639,-36.9965834646228));
#66199=CARTESIAN_POINT('Ctrl Pts',(-27.0586766985272,21.7727686736572,-37.0024475159782));
#66200=CARTESIAN_POINT('Ctrl Pts',(-27.1110160024657,21.8760767729025,-37.0083202097748));
#66201=CARTESIAN_POINT('Ctrl Pts',(-27.1587207064073,21.9815647173778,-37.0141929035713));
#66202=CARTESIAN_POINT('Ctrl Pts',(-27.2016314086062,22.0887733846515,-37.0200655973679));
#66203=CARTESIAN_POINT('Ctrl Pts',(-27.2133796410605,22.1181253243704,-37.0216734426913));
#66204=CARTESIAN_POINT('Ctrl Pts',(-27.224768818873,22.1476061648111,-37.0232812880147));
#66205=CARTESIAN_POINT('Ctrl Pts',(-27.2357963318104,22.1772063207366,-37.024889133338));
#66206=CARTESIAN_POINT('Ctrl Pts',(-27.2821080378936,22.3015166461033,-37.031641522609));
#66207=CARTESIAN_POINT('Ctrl Pts',(-27.322165586825,22.4282767091552,-37.03839391188));
#66208=CARTESIAN_POINT('Ctrl Pts',(-27.355738366958,22.5568912894431,-37.045146301151));
#66209=CARTESIAN_POINT('Ctrl Pts',(-27.3891788643623,22.6849991053951,-37.0518720848066));
#66210=CARTESIAN_POINT('Ctrl Pts',(-27.4161854879993,22.8149467075672,-37.0585978684621));
#66211=CARTESIAN_POINT('Ctrl Pts',(-27.4365769699211,22.9461239354163,-37.0653236521177));
#66212=CARTESIAN_POINT('Ctrl Pts',(-27.4568208581286,23.076351701409,-37.0720007544957));
#66213=CARTESIAN_POINT('Ctrl Pts',(-27.4705449288546,23.2077911962808,-37.0786778568737));
#66214=CARTESIAN_POINT('Ctrl Pts',(-27.4776192945278,23.3398260357622,-37.0853549592517));
#66215=CARTESIAN_POINT('Ctrl Pts',(-27.4813209874302,23.4089138452932,-37.0888487823905));
#66216=CARTESIAN_POINT('Ctrl Pts',(-27.483202820316,23.4781643496993,-37.0923426055294));
#66217=CARTESIAN_POINT('Ctrl Pts',(-27.4832515596232,23.547487335628,-37.0958364286682));
#66218=CARTESIAN_POINT('',(-27.4822753988055,23.5529940695056,-38.3458365164865));
#66219=CARTESIAN_POINT('Ctrl Pts',(-27.4788461937177,23.5474914099673,-37.0958364779651));
#66220=CARTESIAN_POINT('Ctrl Pts',(-27.4733986381108,24.3927224225629,-37.1384830002144));
#66221=CARTESIAN_POINT('Ctrl Pts',(-26.7905005240498,26.5599232774312,-37.2474251595887));
#66222=CARTESIAN_POINT('Ctrl Pts',(-23.2155414968396,28.1901576336606,-37.4226629560879));
#66223=CARTESIAN_POINT('Ctrl Pts',(-19.4656970161889,25.7767199293586,-37.6215498674628));
#66224=CARTESIAN_POINT('Ctrl Pts',(-19.4692127410894,21.3173474599079,-37.8204367788377));
#66225=CARTESIAN_POINT('Ctrl Pts',(-23.222858018441,18.9098254322999,-38.0193236902125));
#66226=CARTESIAN_POINT('Ctrl Pts',(-26.7931104595749,20.5447185682919,-38.1944569232551));
#66227=CARTESIAN_POINT('Ctrl Pts',(-27.4734163905603,22.7098084322925,-38.3032945191725));
#66228=CARTESIAN_POINT('Ctrl Pts',(-27.4788019670004,23.5529908840325,-38.3458364779651));
#66229=CARTESIAN_POINT('',(-27.4847991704008,23.5519704097288,-39.5958364779651));
#66230=CARTESIAN_POINT('Ctrl Pts',(-27.4832515755615,23.5529949647541,-38.3458365273125));
#66231=CARTESIAN_POINT('Ctrl Pts',(-27.4831592318539,23.6854276278161,-38.3525107634145));
#66232=CARTESIAN_POINT('Ctrl Pts',(-27.4763739482618,23.8175957568385,-38.3591849995164));
#66233=CARTESIAN_POINT('Ctrl Pts',(-27.4629996664109,23.9488737300342,-38.3658592356183));
#66234=CARTESIAN_POINT('Ctrl Pts',(-27.449561077883,24.0807829184477,-38.3725655630094));
#66235=CARTESIAN_POINT('Ctrl Pts',(-27.4294700928455,24.2117932052308,-38.3792718904004));
#66236=CARTESIAN_POINT('Ctrl Pts',(-27.4028816673861,24.3412883986546,-38.3859782177915));
#66237=CARTESIAN_POINT('Ctrl Pts',(-27.3761332597264,24.4715627629248,-38.3927248970648));
#66238=CARTESIAN_POINT('Ctrl Pts',(-27.3428090848831,24.6003035844075,-38.3994715763381));
#66239=CARTESIAN_POINT('Ctrl Pts',(-27.3031152843816,24.7269046295938,-38.4062182556113));
#66240=CARTESIAN_POINT('Ctrl Pts',(-27.281779401774,24.7949541739549,-38.4098446747283));
#66241=CARTESIAN_POINT('Ctrl Pts',(-27.2586040313723,24.8623858726676,-38.4134710938453));
#66242=CARTESIAN_POINT('Ctrl Pts',(-27.2336267596423,24.929108324331,-38.4170975129623));
#66243=CARTESIAN_POINT('Ctrl Pts',(-27.1931808121841,25.0371526617359,-38.422969809931));
#66244=CARTESIAN_POINT('Ctrl Pts',(-27.1479091829293,25.1435968936783,-38.4288421068997));
#66245=CARTESIAN_POINT('Ctrl Pts',(-27.0979581740536,25.2479785623515,-38.4347144038685));
#66246=CARTESIAN_POINT('Ctrl Pts',(-27.0480718977184,25.3522249606718,-38.4405790908067));
#66247=CARTESIAN_POINT('Ctrl Pts',(-26.9935184778837,25.4544137417535,-38.4464437777449));
#66248=CARTESIAN_POINT('Ctrl Pts',(-26.9344932323536,25.5540998013233,-38.4523084646831));
#66249=CARTESIAN_POINT('Ctrl Pts',(-26.8755286905936,25.6536833400213,-38.458167120158));
#66250=CARTESIAN_POINT('Ctrl Pts',(-26.8121016801221,25.7507689232456,-38.4640257756328));
#66251=CARTESIAN_POINT('Ctrl Pts',(-26.7444543379561,25.8449341699337,-38.4698844311076));
#66252=CARTESIAN_POINT('Ctrl Pts',(-26.6741646310224,25.9427775940967,-38.4759719308255));
#66253=CARTESIAN_POINT('Ctrl Pts',(-26.5993183676267,26.0374674788321,-38.4820594305434));
#66254=CARTESIAN_POINT('Ctrl Pts',(-26.5202382605485,26.1285608473155,-38.4881469302613));
#66255=CARTESIAN_POINT('Ctrl Pts',(-26.4442191173452,26.2161282530697,-38.4939988003447));
#66256=CARTESIAN_POINT('Ctrl Pts',(-26.3642880921644,26.3003720459029,-38.4998506704282));
#66257=CARTESIAN_POINT('Ctrl Pts',(-26.2807736800725,26.3809314711465,-38.5057025405116));
#66258=CARTESIAN_POINT('Ctrl Pts',(-26.1972719838092,26.461478630485,-38.5115535195945));
#66259=CARTESIAN_POINT('Ctrl Pts',(-26.1101882829092,26.5383422507226,-38.5174044986775));
#66260=CARTESIAN_POINT('Ctrl Pts',(-26.0198878032634,26.6111985660798,-38.5232554777605));
#66261=CARTESIAN_POINT('Ctrl Pts',(-25.9295792047356,26.6840614319209,-38.5291069829028));
#66262=CARTESIAN_POINT('Ctrl Pts',(-25.8360535742644,26.7529160170584,-38.5349584880451));
#66263=CARTESIAN_POINT('Ctrl Pts',(-25.7397085003297,26.8174794233267,-38.5408099931875));
#66264=CARTESIAN_POINT('Ctrl Pts',(-25.6433314322933,26.8820642696967,-38.5466634414872));
#66265=CARTESIAN_POINT('Ctrl Pts',(-25.5441334022921,26.9423548736568,-38.552516889787));
#66266=CARTESIAN_POINT('Ctrl Pts',(-25.4425395764231,26.9981125550059,-38.5583703380868));
#66267=CARTESIAN_POINT('Ctrl Pts',(-25.3408302163134,27.0539336449463,-38.5642304430284));
#66268=CARTESIAN_POINT('Ctrl Pts',(-25.2367199848427,27.1052113242074,-38.5700905479699));
#66269=CARTESIAN_POINT('Ctrl Pts',(-25.1306572496868,27.1517535975481,-38.5759506529115));
#66270=CARTESIAN_POINT('Ctrl Pts',(-25.024523087917,27.1983272141968,-38.581814704267));
#66271=CARTESIAN_POINT('Ctrl Pts',(-24.9164341888335,27.2401589261581,-38.5876787556224));
#66272=CARTESIAN_POINT('Ctrl Pts',(-24.8068557747408,27.277106069139,-38.5935428069779));
#66273=CARTESIAN_POINT('Ctrl Pts',(-24.6971158639395,27.3141076648333,-38.5994155007745));
#66274=CARTESIAN_POINT('Ctrl Pts',(-24.5858824525196,27.3462102097767,-38.605288194571));
#66275=CARTESIAN_POINT('Ctrl Pts',(-24.4736327612511,27.3733217112492,-38.6111608883676));
#66276=CARTESIAN_POINT('Ctrl Pts',(-24.4429006734929,27.3807443868316,-38.6127687336908));
#66277=CARTESIAN_POINT('Ctrl Pts',(-24.412092445677,27.387793246519,-38.614376579014));
#66278=CARTESIAN_POINT('Ctrl Pts',(-24.3812179380884,27.3944670799961,-38.6159844243371));
#66279=CARTESIAN_POINT('Ctrl Pts',(-24.2684556750089,27.4188417704793,-38.6218567213059));
#66280=CARTESIAN_POINT('Ctrl Pts',(-24.1544311219155,27.4382916090648,-38.6277290182746));
#66281=CARTESIAN_POINT('Ctrl Pts',(-24.0396124348488,27.4526897041781,-38.6336013152433));
#66282=CARTESIAN_POINT('Ctrl Pts',(-23.9249425436819,27.4670691405037,-38.6394660021815));
#66283=CARTESIAN_POINT('Ctrl Pts',(-23.8094809715053,27.4764098013506,-38.6453306891197));
#66284=CARTESIAN_POINT('Ctrl Pts',(-23.6937077695654,27.4806354131356,-38.6511953760579));
#66285=CARTESIAN_POINT('Ctrl Pts',(-23.5780536331161,27.4848566791434,-38.6570540315327));
#66286=CARTESIAN_POINT('Ctrl Pts',(-23.4620889150022,27.4839733445224,-38.6629126870076));
#66287=CARTESIAN_POINT('Ctrl Pts',(-23.3462998568208,27.4779608083375,-38.6687713424824));
#66288=CARTESIAN_POINT('Ctrl Pts',(-23.2259879760414,27.4717134171934,-38.6748588422003));
#66289=CARTESIAN_POINT('Ctrl Pts',(-23.1058662089595,27.4599278968983,-38.6809463419182));
#66290=CARTESIAN_POINT('Ctrl Pts',(-22.9864816793478,27.4426363033751,-38.6870338416361));
#66291=CARTESIAN_POINT('Ctrl Pts',(-22.8717181820779,27.4260140177863,-38.6928857117195));
#66292=CARTESIAN_POINT('Ctrl Pts',(-22.7576363580775,27.4043040465735,-38.6987375818029));
#66293=CARTESIAN_POINT('Ctrl Pts',(-22.6447172818115,27.3775877549559,-38.7045894518863));
#66294=CARTESIAN_POINT('Ctrl Pts',(-22.5318153985016,27.3508755311366,-38.7104404309693));
#66295=CARTESIAN_POINT('Ctrl Pts',(-22.4200763130827,27.3191585976763,-38.7162914100522));
#66296=CARTESIAN_POINT('Ctrl Pts',(-22.3099698352141,27.2825692161158,-38.7221423891352));
#66297=CARTESIAN_POINT('Ctrl Pts',(-22.1998534577134,27.2459765448178,-38.7279938942775));
#66298=CARTESIAN_POINT('Ctrl Pts',(-22.0913703718756,27.2045106849263,-38.7338453994198));
#66299=CARTESIAN_POINT('Ctrl Pts',(-21.9849734981023,27.1583532158489,-38.7396969045621));
#66300=CARTESIAN_POINT('Ctrl Pts',(-21.8785412922432,27.1121804188807,-38.7455503528619));
#66301=CARTESIAN_POINT('Ctrl Pts',(-21.7741970550425,27.0613130792125,-38.7514038011617));
#66302=CARTESIAN_POINT('Ctrl Pts',(-21.6723714124572,27.005979879448,-38.7572572494615));
#66303=CARTESIAN_POINT('Ctrl Pts',(-21.5704299720054,26.95058375382,-38.763117354403));
#66304=CARTESIAN_POINT('Ctrl Pts',(-21.4710132064377,26.8907118287525,-38.7689774593445));
#66305=CARTESIAN_POINT('Ctrl Pts',(-21.3745250063084,26.8266375419271,-38.7748375642861));
#66306=CARTESIAN_POINT('Ctrl Pts',(-21.2779718274152,26.7625201050797,-38.7807016156415));
#66307=CARTESIAN_POINT('Ctrl Pts',(-21.1843514741112,26.694194914426,-38.786565666997));
#66308=CARTESIAN_POINT('Ctrl Pts',(-21.0940354446374,26.6219762531982,-38.7924297183524));
#66309=CARTESIAN_POINT('Ctrl Pts',(-21.0035863073649,26.5496511560799,-38.798302412149));
#66310=CARTESIAN_POINT('Ctrl Pts',(-20.9164515232883,26.4734214072164,-38.8041751059456));
#66311=CARTESIAN_POINT('Ctrl Pts',(-20.8329664454832,26.3936387744836,-38.8100477997422));
#66312=CARTESIAN_POINT('Ctrl Pts',(-20.8101096277153,26.3717956242421,-38.8116556450655));
#66313=CARTESIAN_POINT('Ctrl Pts',(-20.7875261506028,26.349686352754,-38.8132634903888));
#66314=CARTESIAN_POINT('Ctrl Pts',(-20.7652223623064,26.327318601416,-38.8148713357121));
#66315=CARTESIAN_POINT('Ctrl Pts',(-20.6837627427124,26.2456253710568,-38.8207436326808));
#66316=CARTESIAN_POINT('Ctrl Pts',(-20.6057641623855,26.1602080637001,-38.8266159296495));
#66317=CARTESIAN_POINT('Ctrl Pts',(-20.5315864355227,26.0713919566021,-38.8324882266182));
#66318=CARTESIAN_POINT('Ctrl Pts',(-20.4575048371029,25.9826909481253,-38.8383529135564));
#66319=CARTESIAN_POINT('Ctrl Pts',(-20.3872345078877,25.8906002133769,-38.8442176004946));
#66320=CARTESIAN_POINT('Ctrl Pts',(-20.3210991061718,25.7954823984199,-38.8500822874328));
#66321=CARTESIAN_POINT('Ctrl Pts',(-20.2550317205764,25.700462406181,-38.8559409429076));
#66322=CARTESIAN_POINT('Ctrl Pts',(-20.19309103858,25.6024218633374,-38.8617995983824));
#66323=CARTESIAN_POINT('Ctrl Pts',(-20.1355605915586,25.5017565552548,-38.8676582538572));
#66324=CARTESIAN_POINT('Ctrl Pts',(-20.0757829546044,25.3971591715735,-38.8737457535751));
#66325=CARTESIAN_POINT('Ctrl Pts',(-20.020767403138,25.2897281401515,-38.879833253293));
#66326=CARTESIAN_POINT('Ctrl Pts',(-19.9707827115671,25.179941092984,-38.8859207530109));
#66327=CARTESIAN_POINT('Ctrl Pts',(-19.9227327838814,25.0744035871713,-38.8917726230943));
#66328=CARTESIAN_POINT('Ctrl Pts',(-19.8793316847739,24.9666894747554,-38.8976244931777));
#66329=CARTESIAN_POINT('Ctrl Pts',(-19.8407710014632,24.8572474731055,-38.9034763632611));
#66330=CARTESIAN_POINT('Ctrl Pts',(-19.8022161893671,24.7478221349955,-38.9093273423441));
#66331=CARTESIAN_POINT('Ctrl Pts',(-19.7685004650167,24.6366698205351,-38.915178321427));
#66332=CARTESIAN_POINT('Ctrl Pts',(-19.7397665065963,24.5242572814432,-38.92102930051));
#66333=CARTESIAN_POINT('Ctrl Pts',(-19.7110299647165,24.4118346353824,-38.9268808056523));
#66334=CARTESIAN_POINT('Ctrl Pts',(-19.6872761815478,24.2981519399773,-38.9327323107946));
#66335=CARTESIAN_POINT('Ctrl Pts',(-19.6685972139659,24.1836883961286,-38.9385838159369));
#66336=CARTESIAN_POINT('Ctrl Pts',(-19.6499120435055,24.0691868414287,-38.9444372642366));
#66337=CARTESIAN_POINT('Ctrl Pts',(-19.6363051061599,23.9539043304483,-38.9502907125364));
#66338=CARTESIAN_POINT('Ctrl Pts',(-19.6278167790031,23.8383267686721,-38.9561441608362));
#66339=CARTESIAN_POINT('Ctrl Pts',(-19.6193187987751,23.7226177701111,-38.9620042657777));
#66340=CARTESIAN_POINT('Ctrl Pts',(-19.615951077515,23.6066134635501,-38.9678643707192));
#66341=CARTESIAN_POINT('Ctrl Pts',(-19.6177018874803,23.4908014535475,-38.9737244756608));
#66342=CARTESIAN_POINT('Ctrl Pts',(-19.6194538765065,23.3749114514046,-38.9795885270162));
#66343=CARTESIAN_POINT('Ctrl Pts',(-19.626331235971,23.2592144153259,-38.9854525783717));
#66344=CARTESIAN_POINT('Ctrl Pts',(-19.6382703646655,23.144192776425,-38.9913166297271));
#66345=CARTESIAN_POINT('Ctrl Pts',(-19.6502270892524,23.0290016185889,-38.9971893235237));
#66346=CARTESIAN_POINT('Ctrl Pts',(-19.6672604112736,22.9144882519072,-39.0030620173202));
#66347=CARTESIAN_POINT('Ctrl Pts',(-19.6892556550669,22.8011249599986,-39.0089347111168));
#66348=CARTESIAN_POINT('Ctrl Pts',(-19.6952775848823,22.7700879870091,-39.0105425564402));
#66349=CARTESIAN_POINT('Ctrl Pts',(-19.7016711591795,22.7391371302837,-39.0121504017636));
#66350=CARTESIAN_POINT('Ctrl Pts',(-19.7084333805734,22.7082818611354,-39.013758247087));
#66351=CARTESIAN_POINT('Ctrl Pts',(-19.7331308882348,22.5955898621899,-39.0196305440557));
#66352=CARTESIAN_POINT('Ctrl Pts',(-19.7628323628056,22.4837966721581,-39.0255028410244));
#66353=CARTESIAN_POINT('Ctrl Pts',(-19.7974586378996,22.3733808349075,-39.0313751379931));
#66354=CARTESIAN_POINT('Ctrl Pts',(-19.8320400400909,22.2631080878129,-39.0372398249313));
#66355=CARTESIAN_POINT('Ctrl Pts',(-19.8715334284444,22.1542095346961,-39.0431045118695));
#66356=CARTESIAN_POINT('Ctrl Pts',(-19.915808653772,22.0471535002815,-39.0489691988077));
#66357=CARTESIAN_POINT('Ctrl Pts',(-19.960038344802,21.9402075662965,-39.0548278542826));
#66358=CARTESIAN_POINT('Ctrl Pts',(-20.009039933974,21.8351007616361,-39.0606865097574));
#66359=CARTESIAN_POINT('Ctrl Pts',(-20.0626337011476,21.7322855647729,-39.0665451652322));
#66360=CARTESIAN_POINT('Ctrl Pts',(-20.1183208880718,21.6254543157619,-39.0726326649501));
#66361=CARTESIAN_POINT('Ctrl Pts',(-20.1789661794692,21.5210977824406,-39.078720164668));
#66362=CARTESIAN_POINT('Ctrl Pts',(-20.2443130194898,21.4197002695693,-39.0848076643859));
#66363=CARTESIAN_POINT('Ctrl Pts',(-20.3071304709695,21.3222275632694,-39.0906595344693));
#66364=CARTESIAN_POINT('Ctrl Pts',(-20.3742920270284,21.2274894463095,-39.0965114045527));
#66365=CARTESIAN_POINT('Ctrl Pts',(-20.4455237352288,21.1358896549918,-39.1023632746362));
#66366=CARTESIAN_POINT('Ctrl Pts',(-20.5167445977539,21.0443038105753,-39.1082142537191));
#66367=CARTESIAN_POINT('Ctrl Pts',(-20.5920341265283,20.9558556679415,-39.1140652328021));
#66368=CARTESIAN_POINT('Ctrl Pts',(-20.6710767591067,20.8709175637319,-39.1199162118851));
#66369=CARTESIAN_POINT('Ctrl Pts',(-20.7501264983784,20.7859718227694,-39.1257677170274));
#66370=CARTESIAN_POINT('Ctrl Pts',(-20.8329297306223,20.7045370502247,-39.1316192221697));
#66371=CARTESIAN_POINT('Ctrl Pts',(-20.9191330567245,20.6269497234933,-39.137470727312));
#66372=CARTESIAN_POINT('Ctrl Pts',(-21.0053650090748,20.5493366316997,-39.1433241756118));
#66373=CARTESIAN_POINT('Ctrl Pts',(-21.0949989933271,20.4755738026527,-39.1491776239116));
#66374=CARTESIAN_POINT('Ctrl Pts',(-21.1876480345647,20.4059578587758,-39.1550310722114));
#66375=CARTESIAN_POINT('Ctrl Pts',(-21.2804024378804,20.3362627464538,-39.1608911771529));
#66376=CARTESIAN_POINT('Ctrl Pts',(-21.3761784112305,20.2707241805854,-39.1667512820945));
#66377=CARTESIAN_POINT('Ctrl Pts',(-21.4745593853769,20.2095958653588,-39.172611387036));
#66378=CARTESIAN_POINT('Ctrl Pts',(-21.5730066129518,20.1484263840378,-39.1784754383915));
#66379=CARTESIAN_POINT('Ctrl Pts',(-21.6740619749411,20.0916732691993,-39.1843394897469));
#66380=CARTESIAN_POINT('Ctrl Pts',(-21.7772852148052,20.0395437865484,-39.1902035411024));
#66381=CARTESIAN_POINT('Ctrl Pts',(-21.8806605851196,19.987337475446,-39.196076234899));
#66382=CARTESIAN_POINT('Ctrl Pts',(-21.9862098344891,19.9397685657942,-39.2019489286955));
#66383=CARTESIAN_POINT('Ctrl Pts',(-22.0934736357243,19.8969958683516,-39.2078216224921));
#66384=CARTESIAN_POINT('Ctrl Pts',(-22.122840670197,19.8852854192923,-39.2094294678154));
#66385=CARTESIAN_POINT('Ctrl Pts',(-22.1523361432092,19.8739341904624,-39.2110373131386));
#66386=CARTESIAN_POINT('Ctrl Pts',(-22.1819504661728,19.8629447797578,-39.2126451584619));
#66387=CARTESIAN_POINT('Ctrl Pts',(-22.2901101855521,19.8228084045515,-39.2185174554306));
#66388=CARTESIAN_POINT('Ctrl Pts',(-22.4002185781596,19.7873677949848,-39.2243897523993));
#66389=CARTESIAN_POINT('Ctrl Pts',(-22.5118302442226,19.7568150202961,-39.230262049368));
#66390=CARTESIAN_POINT('Ctrl Pts',(-22.6232972704304,19.7263018395769,-39.2361267363062));
#66391=CARTESIAN_POINT('Ctrl Pts',(-22.7362633009426,19.7006640053316,-39.2419914232444));
#66392=CARTESIAN_POINT('Ctrl Pts',(-22.8502639751575,19.6800451702318,-39.2478561101826));
#66393=CARTESIAN_POINT('Ctrl Pts',(-22.9641474068155,19.6594475403132,-39.2537147656574));
#66394=CARTESIAN_POINT('Ctrl Pts',(-23.0790629613562,19.6438587157316,-39.2595734211322));
#66395=CARTESIAN_POINT('Ctrl Pts',(-23.1945328146942,19.6333720787141,-39.265432076607));
#66396=CARTESIAN_POINT('Ctrl Pts',(-23.3145130222083,19.6224758244182,-39.2715195763249));
#66397=CARTESIAN_POINT('Ctrl Pts',(-23.4350912755479,19.6170885953447,-39.2776070760428));
#66398=CARTESIAN_POINT('Ctrl Pts',(-23.5557214416796,19.6172563340068,-39.2836945757607));
#66399=CARTESIAN_POINT('Ctrl Pts',(-23.671682360456,19.6174175799869,-39.2895464458441));
#66400=CARTESIAN_POINT('Ctrl Pts',(-23.7876907960239,19.6227117555017,-39.2953983159275));
#66401=CARTESIAN_POINT('Ctrl Pts',(-23.9032589953519,19.6331266163558,-39.3012501860109));
#66402=CARTESIAN_POINT('Ctrl Pts',(-24.0188095983706,19.6435398914526,-39.3071011650939));
#66403=CARTESIAN_POINT('Ctrl Pts',(-24.1339196868251,19.6590722645602,-39.3129521441768));
#66404=CARTESIAN_POINT('Ctrl Pts',(-24.2481054327725,19.6796595114379,-39.3188031232598));
#66405=CARTESIAN_POINT('Ctrl Pts',(-24.3623014451173,19.7002486093073,-39.3246546284021));
#66406=CARTESIAN_POINT('Ctrl Pts',(-24.4755725428977,19.7258934110615,-39.3305061335443));
#66407=CARTESIAN_POINT('Ctrl Pts',(-24.5874446148324,19.7564784763931,-39.3363576386866));
#66408=CARTESIAN_POINT('Ctrl Pts',(-24.699353837047,19.7870736983592,-39.3422110869864));
#66409=CARTESIAN_POINT('Ctrl Pts',(-24.8098627110775,19.8226123370834,-39.3480645352862));
#66410=CARTESIAN_POINT('Ctrl Pts',(-24.918512507155,19.8629291610699,-39.3539179835859));
#66411=CARTESIAN_POINT('Ctrl Pts',(-25.0272858616434,19.9032918340399,-39.3597780885275));
#66412=CARTESIAN_POINT('Ctrl Pts',(-25.1341955305579,19.9484433941431,-39.365638193469));
#66413=CARTESIAN_POINT('Ctrl Pts',(-25.2388028949754,19.9981705125591,-39.3714982984105));
#66414=CARTESIAN_POINT('Ctrl Pts',(-25.3434807059058,20.0479311190771,-39.377362349766));
#66415=CARTESIAN_POINT('Ctrl Pts',(-25.4458527608331,20.1022732261446,-39.3832264011214));
#66416=CARTESIAN_POINT('Ctrl Pts',(-25.5455067063187,20.1609384744485,-39.3890904524768));
#66417=CARTESIAN_POINT('Ctrl Pts',(-25.6453075218272,20.2196901836176,-39.3949631462734));
#66418=CARTESIAN_POINT('Ctrl Pts',(-25.7423818874744,20.282777525787,-39.40083584007));
#66419=CARTESIAN_POINT('Ctrl Pts',(-25.8363479072864,20.3498999052332,-39.4067085338665));
#66420=CARTESIAN_POINT('Ctrl Pts',(-25.8620742316527,20.3682768899062,-39.4083163791899));
#66421=CARTESIAN_POINT('Ctrl Pts',(-25.8875677644883,20.3869561058402,-39.4099242245133));
#66422=CARTESIAN_POINT('Ctrl Pts',(-25.9128211371016,20.4059308902676,-39.4115320698367));
#66423=CARTESIAN_POINT('Ctrl Pts',(-26.0041076019299,20.4745213719348,-39.4173441456261));
#66424=CARTESIAN_POINT('Ctrl Pts',(-26.0925728163968,20.5472171325677,-39.4231562214154));
#66425=CARTESIAN_POINT('Ctrl Pts',(-26.1778188951763,20.6237556488157,-39.4289682972048));
#66426=CARTESIAN_POINT('Ctrl Pts',(-26.2629541132975,20.7001946283997,-39.4347728145169));
#66427=CARTESIAN_POINT('Ctrl Pts',(-26.3448782059138,20.7804661503196,-39.440577331829));
#66428=CARTESIAN_POINT('Ctrl Pts',(-26.423223370057,20.8642652715016,-39.446381849141));
#66429=CARTESIAN_POINT('Ctrl Pts',(-26.5014886760188,20.9479789752173,-39.4521804498378));
#66430=CARTESIAN_POINT('Ctrl Pts',(-26.5761820197674,21.0352128222047,-39.4579790505346));
#66431=CARTESIAN_POINT('Ctrl Pts',(-26.6469703401396,21.1256231136476,-39.4637776512314));
#66432=CARTESIAN_POINT('Ctrl Pts',(-26.7177075464019,21.2159681225474,-39.4695720649337));
#66433=CARTESIAN_POINT('Ctrl Pts',(-26.7845450767361,21.3094846832181,-39.4753664786359));
#66434=CARTESIAN_POINT('Ctrl Pts',(-26.8471888011666,21.4057945034182,-39.4811608923381));
#66435=CARTESIAN_POINT('Ctrl Pts',(-26.9098091768905,21.5020684268105,-39.4869531463337));
#66436=CARTESIAN_POINT('Ctrl Pts',(-26.9682386228485,21.601133186934,-39.4927454003293));
#66437=CARTESIAN_POINT('Ctrl Pts',(-27.0222255848724,21.7025804509383,-39.4985376543249));
#66438=CARTESIAN_POINT('Ctrl Pts',(-27.0762061519759,21.8040156982047,-39.5043292222104));
#66439=CARTESIAN_POINT('Ctrl Pts',(-27.125745083046,21.9078325150411,-39.5101207900959));
#66440=CARTESIAN_POINT('Ctrl Pts',(-27.1706365692537,22.0135975865017,-39.5159123579813));
#66441=CARTESIAN_POINT('Ctrl Pts',(-27.215534152786,22.1193770233584,-39.5217047124986));
#66442=CARTESIAN_POINT('Ctrl Pts',(-27.2557828728013,22.227104851244,-39.5274970670158));
#66443=CARTESIAN_POINT('Ctrl Pts',(-27.2912252184687,22.3363281696325,-39.533289421533));
#66444=CARTESIAN_POINT('Ctrl Pts',(-27.3267014039581,22.4456557728131,-39.5390873065038));
#66445=CARTESIAN_POINT('Ctrl Pts',(-27.3573619224923,22.5564813146062,-39.5448851914746));
#66446=CARTESIAN_POINT('Ctrl Pts',(-27.3830992936658,22.6683371733724,-39.5506830764454));
#66447=CARTESIAN_POINT('Ctrl Pts',(-27.4088501005704,22.7802514244751,-39.5564839880976));
#66448=CARTESIAN_POINT('Ctrl Pts',(-27.4296725671037,22.893196648022,-39.5622848997498));
#66449=CARTESIAN_POINT('Ctrl Pts',(-27.4455107650829,23.0066972951108,-39.568085811402));
#66450=CARTESIAN_POINT('Ctrl Pts',(-27.4613722147019,23.1203645694989,-39.5738952392192));
#66451=CARTESIAN_POINT('Ctrl Pts',(-27.4722347465043,23.2345884752599,-39.5797046670364));
#66452=CARTESIAN_POINT('Ctrl Pts',(-27.4780944751955,23.3488905023242,-39.5855140948537));
#66453=CARTESIAN_POINT('Ctrl Pts',(-27.4815650616504,23.4165890405674,-39.5889548892241));
#66454=CARTESIAN_POINT('Ctrl Pts',(-27.4832816958199,23.4843149981474,-39.5923956835946));
#66455=CARTESIAN_POINT('Ctrl Pts',(-27.4832521568169,23.551969734281,-39.5958364779651));
#66456=CARTESIAN_POINT('',(-27.4832509072098,23.5466778720844,-40.8458364779651));
#66457=CARTESIAN_POINT('Ctrl Pts',(-27.4888435011611,23.5519721755401,-39.5958364779651));
#66458=CARTESIAN_POINT('Ctrl Pts',(-27.4893667048836,23.6476846199245,-39.6006973123806));
#66459=CARTESIAN_POINT('Ctrl Pts',(-27.4427386655007,25.0482753731377,-39.6718537839204));
#66460=CARTESIAN_POINT('Ctrl Pts',(-25.771461580151,27.6376699553484,-39.8093058925872));
#66461=CARTESIAN_POINT('Ctrl Pts',(-21.3120973279039,27.6284153675602,-40.0081928039611));
#66462=CARTESIAN_POINT('Ctrl Pts',(-18.9094079436724,23.8716749048059,-40.2070797153365));
#66463=CARTESIAN_POINT('Ctrl Pts',(-20.771261257099,19.8195745332832,-40.4059666267111));
#66464=CARTESIAN_POINT('Ctrl Pts',(-25.1867719322757,19.1956509329671,-40.6048535380861));
#66465=CARTESIAN_POINT('Ctrl Pts',(-27.333324802602,21.6856728041178,-40.7514768218375));
#66466=CARTESIAN_POINT('Ctrl Pts',(-27.4866705567893,23.2695102944433,-40.8318044684637));
#66467=CARTESIAN_POINT('Ctrl Pts',(-27.4840929910064,23.5466771067236,-40.8458364779651));
#66468=CARTESIAN_POINT('',(-27.483252531009,23.5501791140891,-42.0958364779359));
#66469=CARTESIAN_POINT('Ctrl Pts',(-27.4832509072098,23.5466778720844,-40.8458364779651));
#66470=CARTESIAN_POINT('Ctrl Pts',(-27.4833546239329,23.6607915913766,-40.8516149565601));
#66471=CARTESIAN_POINT('Ctrl Pts',(-27.4784877326466,23.7750600714861,-40.8573934351551));
#66472=CARTESIAN_POINT('Ctrl Pts',(-27.46863658494,23.8890082124863,-40.8631719137501));
#66473=CARTESIAN_POINT('Ctrl Pts',(-27.4587306022987,24.0035906287068,-40.8689825573786));
#66474=CARTESIAN_POINT('Ctrl Pts',(-27.4437846550542,24.1178486950974,-40.8747932010072));
#66475=CARTESIAN_POINT('Ctrl Pts',(-27.4238380713898,24.2312988345701,-40.8806038446358));
#66476=CARTESIAN_POINT('Ctrl Pts',(-27.4040275805656,24.3439749190992,-40.8863748430295));
#66477=CARTESIAN_POINT('Ctrl Pts',(-27.3792845583178,24.4558536426567,-40.8921458414232));
#66478=CARTESIAN_POINT('Ctrl Pts',(-27.3496994383711,24.5664671760205,-40.8979168398169));
#66479=CARTESIAN_POINT('Ctrl Pts',(-27.3201200368547,24.6770593291845,-40.9036867227494));
#66480=CARTESIAN_POINT('Ctrl Pts',(-27.2857005075728,24.7863863667189,-40.909456605682));
#66481=CARTESIAN_POINT('Ctrl Pts',(-27.2465818921875,24.8939929302666,-40.9152264886145));
#66482=CARTESIAN_POINT('Ctrl Pts',(-27.2074607445555,25.0016064594586,-40.9209967450461));
#66483=CARTESIAN_POINT('Ctrl Pts',(-27.163640052765,25.1074988932365,-40.9267670014778));
#66484=CARTESIAN_POINT('Ctrl Pts',(-27.1153096941662,25.2112330939848,-40.9325372579094));
#66485=CARTESIAN_POINT('Ctrl Pts',(-27.0663881276119,25.3162362380332,-40.9383780998199));
#66486=CARTESIAN_POINT('Ctrl Pts',(-27.0128460033438,25.4190275828371,-40.9442189417305));
#66487=CARTESIAN_POINT('Ctrl Pts',(-26.9549284064541,25.5191789365728,-40.950059783641));
#66488=CARTESIAN_POINT('Ctrl Pts',(-26.8976284850674,25.6182622032136,-40.9558383345526));
#66489=CARTESIAN_POINT('Ctrl Pts',(-26.836046253187,25.7147611904133,-40.9616168854642));
#66490=CARTESIAN_POINT('Ctrl Pts',(-26.7704622490776,25.8082911443112,-40.9673954363758));
#66491=CARTESIAN_POINT('Ctrl Pts',(-26.7038177819236,25.90333343435,-40.9732674237858));
#66492=CARTESIAN_POINT('Ctrl Pts',(-26.6330412851277,25.995309476246,-40.9791394111958));
#66493=CARTESIAN_POINT('Ctrl Pts',(-26.5584682167693,26.0838522222665,-40.9850113986058));
#66494=CARTESIAN_POINT('Ctrl Pts',(-26.4838951484109,26.172394968287,-40.9908833860158));
#66495=CARTESIAN_POINT('Ctrl Pts',(-26.4055258673103,26.2575041323493,-40.9967553734258));
#66496=CARTESIAN_POINT('Ctrl Pts',(-26.3237321843897,26.3388542630434,-41.0026273608358));
#66497=CARTESIAN_POINT('Ctrl Pts',(-26.2419341894797,26.4202086823439,-41.0084996578045));
#66498=CARTESIAN_POINT('Ctrl Pts',(-26.1564165747446,26.4980972726454,-41.0143719547732));
#66499=CARTESIAN_POINT('Ctrl Pts',(-26.0675050802241,26.5721606386557,-41.0202442517419));
#66500=CARTESIAN_POINT('Ctrl Pts',(-25.9787088079395,26.6461280244254,-41.0261089386801));
#66501=CARTESIAN_POINT('Ctrl Pts',(-25.8865277169977,26.7162797818324,-41.0319736256183));
#66502=CARTESIAN_POINT('Ctrl Pts',(-25.791324869684,26.7822927195472,-41.0378383125565));
#66503=CARTESIAN_POINT('Ctrl Pts',(-25.6962199325391,26.848237767088,-41.0436969680313));
#66504=CARTESIAN_POINT('Ctrl Pts',(-25.5980997580374,26.9100522272332,-41.0495556235062));
#66505=CARTESIAN_POINT('Ctrl Pts',(-25.4973604961,26.9674530781866,-41.055414278981));
#66506=CARTESIAN_POINT('Ctrl Pts',(-25.3926862698612,27.0270960569361,-41.0615017786989));
#66507=CARTESIAN_POINT('Ctrl Pts',(-25.2851845266623,27.0819733074568,-41.0675892784168));
#66508=CARTESIAN_POINT('Ctrl Pts',(-25.1753332439945,27.1318166702389,-41.0736767781347));
#66509=CARTESIAN_POINT('Ctrl Pts',(-25.069733989053,27.1797307395674,-41.0795286482181));
#66510=CARTESIAN_POINT('Ctrl Pts',(-24.9619641119919,27.2229931830438,-41.0853805183015));
#66511=CARTESIAN_POINT('Ctrl Pts',(-24.8524725763665,27.2614129910726,-41.0912323883849));
#66512=CARTESIAN_POINT('Ctrl Pts',(-24.7429977118231,27.2998269493362,-41.0970833674679));
#66513=CARTESIAN_POINT('Ctrl Pts',(-24.6318020998893,27.3333996013769,-41.1029343465509));
#66514=CARTESIAN_POINT('Ctrl Pts',(-24.5193526755131,27.3619888698018,-41.1087853256338));
#66515=CARTESIAN_POINT('Ctrl Pts',(-24.4068931408517,27.3905807086771,-41.1146368307761));
#66516=CARTESIAN_POINT('Ctrl Pts',(-24.2931799703128,27.4141881713818,-41.1204883359184));
#66517=CARTESIAN_POINT('Ctrl Pts',(-24.1786924828701,27.4327198178108,-41.1263398410607));
#66518=CARTESIAN_POINT('Ctrl Pts',(-24.064166976625,27.4512576181963,-41.1321932893605));
#66519=CARTESIAN_POINT('Ctrl Pts',(-23.9488670500374,27.4647161846421,-41.1380467376603));
#66520=CARTESIAN_POINT('Ctrl Pts',(-23.8332786601519,27.4730557654303,-41.14390018596));
#66521=CARTESIAN_POINT('Ctrl Pts',(-23.7175588211674,27.4814048301327,-41.1497602909016));
#66522=CARTESIAN_POINT('Ctrl Pts',(-23.6015502766721,27.4846232600771,-41.1556203958431));
#66523=CARTESIAN_POINT('Ctrl Pts',(-23.4857406157279,27.4827234105054,-41.1614805007847));
#66524=CARTESIAN_POINT('Ctrl Pts',(-23.3698529642249,27.4808222815039,-41.1673445521402));
#66525=CARTESIAN_POINT('Ctrl Pts',(-23.2541648745799,27.4737960346408,-41.1732086034956));
#66526=CARTESIAN_POINT('Ctrl Pts',(-23.1391586956569,27.4617088919227,-41.1790726548511));
#66527=CARTESIAN_POINT('Ctrl Pts',(-23.023983020584,27.4496039351692,-41.1849453486477));
#66528=CARTESIAN_POINT('Ctrl Pts',(-22.9094916692907,27.4324232574498,-41.1908180424442));
#66529=CARTESIAN_POINT('Ctrl Pts',(-22.7961567774259,27.410282142124,-41.1966907362408));
#66530=CARTESIAN_POINT('Ctrl Pts',(-22.7651275798946,27.4042202751234,-41.1982985815641));
#66531=CARTESIAN_POINT('Ctrl Pts',(-22.7341849768338,27.3977868747737,-41.1999064268875));
#66532=CARTESIAN_POINT('Ctrl Pts',(-22.703338435691,27.3909849506465,-41.2015142722108));
#66533=CARTESIAN_POINT('Ctrl Pts',(-22.5906783138372,27.3661424375923,-41.2073865691795));
#66534=CARTESIAN_POINT('Ctrl Pts',(-22.4789234398692,27.3362971184697,-41.2132588661482));
#66535=CARTESIAN_POINT('Ctrl Pts',(-22.3685522553774,27.3015287754482,-41.2191311631169));
#66536=CARTESIAN_POINT('Ctrl Pts',(-22.2583241031752,27.2668054894379,-41.2249958500551));
#66537=CARTESIAN_POINT('Ctrl Pts',(-22.1494764651573,27.227171989814,-41.2308605369933));
#66538=CARTESIAN_POINT('Ctrl Pts',(-22.0424774981683,27.182759028354,-41.2367252239315));
#66539=CARTESIAN_POINT('Ctrl Pts',(-21.9355885729184,27.1383917428446,-41.2425838794063));
#66540=CARTESIAN_POINT('Ctrl Pts',(-21.8305449165322,27.0892549299612,-41.2484425348812));
#66541=CARTESIAN_POINT('Ctrl Pts',(-21.7277987758217,27.035528892,-41.254301190356));
#66542=CARTESIAN_POINT('Ctrl Pts',(-21.6210392803576,26.9797042676748,-41.2603886900739));
#66543=CARTESIAN_POINT('Ctrl Pts',(-21.5167608792292,26.9189247277489,-41.2664761897918));
#66544=CARTESIAN_POINT('Ctrl Pts',(-21.415447546628,26.8534474511224,-41.2725636895097));
#66545=CARTESIAN_POINT('Ctrl Pts',(-21.3180557622218,26.7905046118634,-41.2784155595931));
#66546=CARTESIAN_POINT('Ctrl Pts',(-21.2234041554162,26.7232211908264,-41.2842674296765));
#66547=CARTESIAN_POINT('Ctrl Pts',(-21.1318961096235,26.6518716597996,-41.2901192997599));
#66548=CARTESIAN_POINT('Ctrl Pts',(-21.0404019967627,26.5805329923876,-41.2959702788429));
#66549=CARTESIAN_POINT('Ctrl Pts',(-20.9520508191438,26.5051297000739,-41.3018212579259));
#66550=CARTESIAN_POINT('Ctrl Pts',(-20.8672145069952,26.4259778242108,-41.3076722370088));
#66551=CARTESIAN_POINT('Ctrl Pts',(-20.782370567246,26.3468188318324,-41.3135237421511));
#66552=CARTESIAN_POINT('Ctrl Pts',(-20.7010424234609,26.2639108679335,-41.3193752472934));
#66553=CARTESIAN_POINT('Ctrl Pts',(-20.6235660979596,26.1776077643558,-41.3252267524357));
#66554=CARTESIAN_POINT('Ctrl Pts',(-20.5460640442569,26.0912760013956,-41.3310802007355));
#66555=CARTESIAN_POINT('Ctrl Pts',(-20.4724166282632,26.0015471643394,-41.3369336490353));
#66556=CARTESIAN_POINT('Ctrl Pts',(-20.4029199741495,25.9088086095136,-41.3427870973351));
#66557=CARTESIAN_POINT('Ctrl Pts',(-20.3333442872495,25.8159645908137,-41.3486472022766));
#66558=CARTESIAN_POINT('Ctrl Pts',(-20.2679290318867,25.7201043537337,-41.3545073072181));
#66559=CARTESIAN_POINT('Ctrl Pts',(-20.2069273759473,25.6216447936644,-41.3603674121597));
#66560=CARTESIAN_POINT('Ctrl Pts',(-20.1458846392107,25.5231189272441,-41.3662314635151));
#66561=CARTESIAN_POINT('Ctrl Pts',(-20.0892616217658,25.4219906120896,-41.3720955148705));
#66562=CARTESIAN_POINT('Ctrl Pts',(-20.03726502257,25.3187003711108,-41.377959566226));
#66563=CARTESIAN_POINT('Ctrl Pts',(-19.9851917907664,25.2152579009354,-41.3838322600225));
#66564=CARTESIAN_POINT('Ctrl Pts',(-19.9377587541865,25.1096475214803,-41.3897049538191));
#66565=CARTESIAN_POINT('Ctrl Pts',(-19.8951241323392,25.0023287639316,-41.3955776476156));
#66566=CARTESIAN_POINT('Ctrl Pts',(-19.8834514860675,24.9729466833382,-41.397185492939));
#66567=CARTESIAN_POINT('Ctrl Pts',(-19.8721382250183,24.9434366266,-41.3987933382623));
#66568=CARTESIAN_POINT('Ctrl Pts',(-19.8611869347455,24.9138081856406,-41.4004011835857));
#66569=CARTESIAN_POINT('Ctrl Pts',(-19.8211897859282,24.8055969034308,-41.4062734805544));
#66570=CARTESIAN_POINT('Ctrl Pts',(-19.785890906653,24.6954429926919,-41.4121457775231));
#66571=CARTESIAN_POINT('Ctrl Pts',(-19.7554817928044,24.5837921000058,-41.4180180744918));
#66572=CARTESIAN_POINT('Ctrl Pts',(-19.7251120867523,24.4722858980096,-41.42388276143));
#66573=CARTESIAN_POINT('Ctrl Pts',(-19.699619652239,24.3592869671422,-41.4297474483682));
#66574=CARTESIAN_POINT('Ctrl Pts',(-19.6791475442211,24.2452598524908,-41.4356121353064));
#66575=CARTESIAN_POINT('Ctrl Pts',(-19.6586964904848,24.1313500075889,-41.4414707907813));
#66576=CARTESIAN_POINT('Ctrl Pts',(-19.6432555661998,24.0164144866021,-41.4473294462561));
#66577=CARTESIAN_POINT('Ctrl Pts',(-19.6329175385933,23.900931233396,-41.4531881017309));
#66578=CARTESIAN_POINT('Ctrl Pts',(-19.6221756985229,23.7809371026034,-41.4592756014488));
#66579=CARTESIAN_POINT('Ctrl Pts',(-19.6169436487515,23.6603520161677,-41.4653631011667));
#66580=CARTESIAN_POINT('Ctrl Pts',(-19.6172666289234,23.5397221657949,-41.4714506008846));
#66581=CARTESIAN_POINT('Ctrl Pts',(-19.6175771074602,23.4237615505545,-41.477302470968));
#66582=CARTESIAN_POINT('Ctrl Pts',(-19.6230205724317,23.3077600242436,-41.4831543410514));
#66583=CARTESIAN_POINT('Ctrl Pts',(-19.6335841519522,23.192205323732,-41.4890062111348));
#66584=CARTESIAN_POINT('Ctrl Pts',(-19.6441461230718,23.0766682174745,-41.4948571902178));
#66585=CARTESIAN_POINT('Ctrl Pts',(-19.6598266210551,22.9615782132978,-41.5007081693008));
#66586=CARTESIAN_POINT('Ctrl Pts',(-19.6805607990657,22.8474190560924,-41.5065591483838));
#66587=CARTESIAN_POINT('Ctrl Pts',(-19.7012968412784,22.73324963488,-41.5124106535261));
#66588=CARTESIAN_POINT('Ctrl Pts',(-19.7270873928964,22.6200116337642,-41.5182621586684));
#66589=CARTESIAN_POINT('Ctrl Pts',(-19.7578164035634,22.5081790150707,-41.5241136638107));
#66590=CARTESIAN_POINT('Ctrl Pts',(-19.7885556186658,22.3963092591992,-41.5299671121105));
#66591=CARTESIAN_POINT('Ctrl Pts',(-19.8242364442935,22.2858462121451,-41.5358205604103));
#66592=CARTESIAN_POINT('Ctrl Pts',(-19.864693058738,22.1772483906579,-41.54167400871));
#66593=CARTESIAN_POINT('Ctrl Pts',(-19.9051956811382,22.0685270698657,-41.5475341136516));
#66594=CARTESIAN_POINT('Ctrl Pts',(-19.9504847882875,21.9616755960297,-41.5533942185932));
#66595=CARTESIAN_POINT('Ctrl Pts',(-20.0003464870739,21.8571323131722,-41.5592543235347));
#66596=CARTESIAN_POINT('Ctrl Pts',(-20.0502417645936,21.7525186269568,-41.5651183748902));
#66597=CARTESIAN_POINT('Ctrl Pts',(-20.1047155715402,21.6502165908703,-41.5709824262457));
#66598=CARTESIAN_POINT('Ctrl Pts',(-20.1635090181477,21.5506382255214,-41.5768464776011));
#66599=CARTESIAN_POINT('Ctrl Pts',(-20.2223891145591,21.4509131015399,-41.5827191713977));
#66600=CARTESIAN_POINT('Ctrl Pts',(-20.2856013316514,21.3539200047846,-41.5885918651943));
#66601=CARTESIAN_POINT('Ctrl Pts',(-20.3528445824797,21.26004044407,-41.5944645589909));
#66602=CARTESIAN_POINT('Ctrl Pts',(-20.3712546597133,21.234337790761,-41.5960724043141));
#66603=CARTESIAN_POINT('Ctrl Pts',(-20.3899666683729,21.2088683177379,-41.5976802496373));
#66604=CARTESIAN_POINT('Ctrl Pts',(-20.4089739362136,21.183639385112,-41.5992880949606));
#66605=CARTESIAN_POINT('Ctrl Pts',(-20.4783937489969,21.091496327294,-41.6051603919293));
#66606=CARTESIAN_POINT('Ctrl Pts',(-20.5519875416169,21.0022559293968,-41.611032688898));
#66607=CARTESIAN_POINT('Ctrl Pts',(-20.6294838957706,20.9163201909905,-41.6169049858667));
#66608=CARTESIAN_POINT('Ctrl Pts',(-20.7068798208039,20.8304958184764,-41.6227696728049));
#66609=CARTESIAN_POINT('Ctrl Pts',(-20.7881679757107,20.7479678931038,-41.6286343597431));
#66610=CARTESIAN_POINT('Ctrl Pts',(-20.8730348581837,20.669107875721,-41.6344990466813));
#66611=CARTESIAN_POINT('Ctrl Pts',(-20.9578144603808,20.5903289609293,-41.6403577021561));
#66612=CARTESIAN_POINT('Ctrl Pts',(-21.0461651684401,20.5152107307009,-41.6462163576309));
#66613=CARTESIAN_POINT('Ctrl Pts',(-21.1377350247873,20.4440895805811,-41.6520750131057));
#66614=CARTESIAN_POINT('Ctrl Pts',(-21.2328816803773,20.3701903756948,-41.6581625128236));
#66615=CARTESIAN_POINT('Ctrl Pts',(-21.3315037920983,20.3006072132542,-41.6642500125415));
#66616=CARTESIAN_POINT('Ctrl Pts',(-21.4331662936495,20.2356733939028,-41.6703375122594));
#66617=CARTESIAN_POINT('Ctrl Pts',(-21.530893731678,20.1732529762484,-41.6761893823428));
#66618=CARTESIAN_POINT('Ctrl Pts',(-21.6314301856473,20.115128912036,-41.6820412524262));
#66619=CARTESIAN_POINT('Ctrl Pts',(-21.7343583565453,20.0615540143871,-41.6878931225096));
#66620=CARTESIAN_POINT('Ctrl Pts',(-21.8372708556935,20.0079872740036,-41.6937441015925));
#66621=CARTESIAN_POINT('Ctrl Pts',(-21.9425739811191,19.9589685137791,-41.6995950806755));
#66622=CARTESIAN_POINT('Ctrl Pts',(-22.0498256976651,19.9147046616029,-41.7054460597585));
#66623=CARTESIAN_POINT('Ctrl Pts',(-22.1570870571728,19.8704368296803,-41.7112975649008));
#66624=CARTESIAN_POINT('Ctrl Pts',(-22.2662969739351,19.8309249133739,-41.717149070043));
#66625=CARTESIAN_POINT('Ctrl Pts',(-22.3769939653576,19.7963274743019,-41.7230005751853));
#66626=CARTESIAN_POINT('Ctrl Pts',(-22.4877277168412,19.7617185461735,-41.7288540234851));
#66627=CARTESIAN_POINT('Ctrl Pts',(-22.5999491305731,19.7320274636421,-41.7347074717849));
#66628=CARTESIAN_POINT('Ctrl Pts',(-22.7131828150561,19.7073625658628,-41.7405609200846));
#66629=CARTESIAN_POINT('Ctrl Pts',(-22.8265452708263,19.682669618739,-41.7464210250262));
#66630=CARTESIAN_POINT('Ctrl Pts',(-22.9409218909,19.6630143530916,-41.7522811299677));
#66631=CARTESIAN_POINT('Ctrl Pts',(-23.0558282708018,19.6484537605835,-41.7581412349092));
#66632=CARTESIAN_POINT('Ctrl Pts',(-23.1708120329589,19.6338833624276,-41.7640052862647));
#66633=CARTESIAN_POINT('Ctrl Pts',(-23.28632585433,19.6244145027907,-41.7698693376201));
#66634=CARTESIAN_POINT('Ctrl Pts',(-23.4018831541704,19.6200520879747,-41.7757333889756));
#66635=CARTESIAN_POINT('Ctrl Pts',(-23.5176107624034,19.61568324383,-41.7816060827721));
#66636=CARTESIAN_POINT('Ctrl Pts',(-23.633381565172,19.6164358620342,-41.7874787765687));
#66637=CARTESIAN_POINT('Ctrl Pts',(-23.7487118424519,19.6222628547763,-41.7933514703652));
#66638=CARTESIAN_POINT('Ctrl Pts',(-23.7802873431325,19.6238581879155,-41.7949593156886));
#66639=CARTESIAN_POINT('Ctrl Pts',(-23.8118298720617,19.6258335848591,-41.796567161012));
#66640=CARTESIAN_POINT('Ctrl Pts',(-23.8433296304232,19.6281874105876,-41.7981750063354));
#66641=CARTESIAN_POINT('Ctrl Pts',(-23.9583754826885,19.6367842348528,-41.8040473033041));
#66642=CARTESIAN_POINT('Ctrl Pts',(-24.0732354915104,19.6504617091263,-41.8099196002728));
#66643=CARTESIAN_POINT('Ctrl Pts',(-24.1874247348063,19.6692087824456,-41.8157918972415));
#66644=CARTESIAN_POINT('Ctrl Pts',(-24.3014659979123,19.6879315610469,-41.8216565841797));
#66645=CARTESIAN_POINT('Ctrl Pts',(-24.4148378199795,19.7117108073719,-41.827521271118));
#66646=CARTESIAN_POINT('Ctrl Pts',(-24.5270582234763,19.7404835570053,-41.8333859580562));
#66647=CARTESIAN_POINT('Ctrl Pts',(-24.6391632153123,19.7692267156667,-41.839244613531));
#66648=CARTESIAN_POINT('Ctrl Pts',(-24.7501187459138,19.8029530608005,-41.8451032690058));
#66649=CARTESIAN_POINT('Ctrl Pts',(-24.859451552075,19.8415483206477,-41.8509619244806));
#66650=CARTESIAN_POINT('Ctrl Pts',(-24.9730549939445,19.881651145339,-41.8570494241985));
#66651=CARTESIAN_POINT('Ctrl Pts',(-25.0849059082626,19.9270109334973,-41.8631369239164));
#66652=CARTESIAN_POINT('Ctrl Pts',(-25.1944887118264,19.9774418196715,-41.8692244236343));
#66653=CARTESIAN_POINT('Ctrl Pts',(-25.2998298797188,20.0259206710484,-41.8750762937177));
#66654=CARTESIAN_POINT('Ctrl Pts',(-25.403074845574,20.0790851558375,-41.8809281638011));
#66655=CARTESIAN_POINT('Ctrl Pts',(-25.5037853456642,20.1367208495881,-41.8867800338845));
#66656=CARTESIAN_POINT('Ctrl Pts',(-25.604480511665,20.1943477677801,-41.8926310129675));
#66657=CARTESIAN_POINT('Ctrl Pts',(-25.7026416204997,20.2564443360485,-41.8984819920504));
#66658=CARTESIAN_POINT('Ctrl Pts',(-25.7978556415216,20.3227505160954,-41.9043329711334));
#66659=CARTESIAN_POINT('Ctrl Pts',(-25.8930782232,20.3890626577058,-41.9101844762757));
#66660=CARTESIAN_POINT('Ctrl Pts',(-25.9853528510759,20.459584927236,-41.9160359814179));
#66661=CARTESIAN_POINT('Ctrl Pts',(-26.0742966736938,20.534014780913,-41.9218874865602));
#66662=CARTESIAN_POINT('Ctrl Pts',(-26.1632700326189,20.6084693511241,-41.9277409348599));
#66663=CARTESIAN_POINT('Ctrl Pts',(-26.2489100700422,20.6868338205726,-41.9335943831597));
#66664=CARTESIAN_POINT('Ctrl Pts',(-26.330868669157,20.7687667963216,-41.9394478314594));
#66665=CARTESIAN_POINT('Ctrl Pts',(-26.412920472996,20.8507929476554,-41.945307936401));
#66666=CARTESIAN_POINT('Ctrl Pts',(-26.4912821896849,20.9363954128342,-41.9511680413425));
#66667=CARTESIAN_POINT('Ctrl Pts',(-26.5656440300273,21.0251974606551,-41.957028146284));
#66668=CARTESIAN_POINT('Ctrl Pts',(-26.640055948415,21.1140593110972,-41.9628921976394));
#66669=CARTESIAN_POINT('Ctrl Pts',(-26.7104623763278,21.2061247070886,-41.9687562489948));
#66670=CARTESIAN_POINT('Ctrl Pts',(-26.7765961684914,21.3009869321489,-41.9746203003502));
#66671=CARTESIAN_POINT('Ctrl Pts',(-26.8428274286634,21.395988965193,-41.9804929941468));
#66672=CARTESIAN_POINT('Ctrl Pts',(-26.9047732651099,21.4937957060384,-41.9863656879434));
#66673=CARTESIAN_POINT('Ctrl Pts',(-26.9622118224166,21.5939747399547,-41.9922383817399));
#66674=CARTESIAN_POINT('Ctrl Pts',(-26.9779375385788,21.6214020836527,-41.9938462270634));
#66675=CARTESIAN_POINT('Ctrl Pts',(-26.993325678056,21.6490071282614,-41.9954540723869));
#66676=CARTESIAN_POINT('Ctrl Pts',(-27.0083723197421,21.6767807460749,-41.9970619177103));
#66677=CARTESIAN_POINT('Ctrl Pts',(-27.0662475677887,21.7836089043874,-42.0032463174493));
#66678=CARTESIAN_POINT('Ctrl Pts',(-27.1192437917329,21.8932593022833,-42.0094307171883));
#66679=CARTESIAN_POINT('Ctrl Pts',(-27.167091389344,22.0052717299383,-42.0156151169273));
#66680=CARTESIAN_POINT('Ctrl Pts',(-27.2148506879968,22.1170774475144,-42.0217881038456));
#66681=CARTESIAN_POINT('Ctrl Pts',(-27.2574801505841,22.2312361925119,-42.0279610907638));
#66682=CARTESIAN_POINT('Ctrl Pts',(-27.294755889838,22.3472630883283,-42.0341340776821));
#66683=CARTESIAN_POINT('Ctrl Pts',(-27.331942379294,22.463012179406,-42.0402922845357));
#66684=CARTESIAN_POINT('Ctrl Pts',(-27.3638005933607,22.5806201732055,-42.0464504913893));
#66685=CARTESIAN_POINT('Ctrl Pts',(-27.3901549413329,22.6995830985704,-42.052608698243));
#66686=CARTESIAN_POINT('Ctrl Pts',(-27.4164708538347,22.8183725270991,-42.0587579239001));
#66687=CARTESIAN_POINT('Ctrl Pts',(-27.4372988102862,22.9385126128449,-42.0649071495573));
#66688=CARTESIAN_POINT('Ctrl Pts',(-27.4525127845195,23.0594838293304,-42.0710563752145));
#66689=CARTESIAN_POINT('Ctrl Pts',(-27.4676988927091,23.1802334739147,-42.077194337898));
#66690=CARTESIAN_POINT('Ctrl Pts',(-27.4772914712536,23.3018108695333,-42.0833323005816));
#66691=CARTESIAN_POINT('Ctrl Pts',(-27.4812155263533,23.4236866017564,-42.0894702632651));
#66692=CARTESIAN_POINT('Ctrl Pts',(-27.4825721859069,23.4658225739292,-42.0915923348221));
#66693=CARTESIAN_POINT('Ctrl Pts',(-27.4832517435385,23.507994117478,-42.093714406379));
#66694=CARTESIAN_POINT('Ctrl Pts',(-27.483252531009,23.5501791140891,-42.095836477936));
#66695=CARTESIAN_POINT('',(-27.4832508841044,23.5538525231951,-43.3458364779651));
#66696=CARTESIAN_POINT('Ctrl Pts',(-27.483252531009,23.5501791146685,-42.0958364779651));
#66697=CARTESIAN_POINT('Ctrl Pts',(-27.4832548023492,23.6718563556103,-42.1019573226462));
#66698=CARTESIAN_POINT('Ctrl Pts',(-27.4776061777862,23.7934277859455,-42.1080781673273));
#66699=CARTESIAN_POINT('Ctrl Pts',(-27.4663618573772,23.914363434166,-42.1141990120083));
#66700=CARTESIAN_POINT('Ctrl Pts',(-27.4551024321348,24.0354615388757,-42.120328079004));
#66701=CARTESIAN_POINT('Ctrl Pts',(-27.4382323502158,24.1559218053875,-42.1264571459996));
#66702=CARTESIAN_POINT('Ctrl Pts',(-27.4158581845192,24.2752228323601,-42.1325862129952));
#66703=CARTESIAN_POINT('Ctrl Pts',(-27.3934308955725,24.3948071171923,-42.1387298323081));
#66704=CARTESIAN_POINT('Ctrl Pts',(-27.3654734665504,24.5132263115375,-42.144873451621));
#66705=CARTESIAN_POINT('Ctrl Pts',(-27.3321431398045,24.6299712118543,-42.1510170709339));
#66706=CARTESIAN_POINT('Ctrl Pts',(-27.2987695721189,24.7468675706085,-42.1571686606419));
#66707=CARTESIAN_POINT('Ctrl Pts',(-27.2600093126576,24.8620849663055,-42.1633202503499));
#66708=CARTESIAN_POINT('Ctrl Pts',(-27.2160681697929,24.9751331258042,-42.1694718400579));
#66709=CARTESIAN_POINT('Ctrl Pts',(-27.172028412201,25.0884349931647,-42.1756372354455));
#66710=CARTESIAN_POINT('Ctrl Pts',(-27.1227846735459,25.1995575690667,-42.1818026308332));
#66711=CARTESIAN_POINT('Ctrl Pts',(-27.0685897512435,25.3080330098923,-42.1879680262208));
#66712=CARTESIAN_POINT('Ctrl Pts',(-27.0452055255798,25.3548383945937,-42.1906282938423));
#66713=CARTESIAN_POINT('Ctrl Pts',(-27.0209000560249,25.4011512922844,-42.1932885614637));
#66714=CARTESIAN_POINT('Ctrl Pts',(-26.9956961240515,25.4469358083337,-42.1959488290852));
#66715=CARTESIAN_POINT('Ctrl Pts',(-26.9400607540866,25.5480009314964,-42.2018211260539));
#66716=CARTESIAN_POINT('Ctrl Pts',(-26.8798815979984,25.646785363983,-42.2076934230227));
#66717=CARTESIAN_POINT('Ctrl Pts',(-26.8153702541408,25.7428526453869,-42.2135657199914));
#66718=CARTESIAN_POINT('Ctrl Pts',(-26.7509425118614,25.8387954312236,-42.2194304069296));
#66719=CARTESIAN_POINT('Ctrl Pts',(-26.6821939747129,25.9320277283877,-42.2252950938678));
#66720=CARTESIAN_POINT('Ctrl Pts',(-26.6093822343018,26.0221373313206,-42.231159780806));
#66721=CARTESIAN_POINT('Ctrl Pts',(-26.5366453762077,26.1121542621677,-42.2370184362808));
#66722=CARTESIAN_POINT('Ctrl Pts',(-26.4598538848487,26.1990545670127,-42.2428770917557));
#66723=CARTESIAN_POINT('Ctrl Pts',(-26.3793083957282,26.2824552910397,-42.2487357472305));
#66724=CARTESIAN_POINT('Ctrl Pts',(-26.2956167288591,26.3691137208055,-42.2548232469484));
#66725=CARTESIAN_POINT('Ctrl Pts',(-26.2078720701821,26.4519932254442,-42.2609107466663));
#66726=CARTESIAN_POINT('Ctrl Pts',(-26.1164577615215,26.530702114963,-42.2669982463842));
#66727=CARTESIAN_POINT('Ctrl Pts',(-26.0285818382629,26.6063644093725,-42.2728501164676));
#66728=CARTESIAN_POINT('Ctrl Pts',(-25.937315408431,26.678172655439,-42.278701986551));
#66729=CARTESIAN_POINT('Ctrl Pts',(-25.8430356531267,26.7458173578359,-42.2845538566345));
#66730=CARTESIAN_POINT('Ctrl Pts',(-25.7487702527725,26.8134517607118,-42.2904048357174));
#66731=CARTESIAN_POINT('Ctrl Pts',(-25.651492774981,26.876923639469,-42.2962558148004));
#66732=CARTESIAN_POINT('Ctrl Pts',(-25.5516114006621,26.9359654075305,-42.3021067938834));
#66733=CARTESIAN_POINT('Ctrl Pts',(-25.4517210460465,26.995012484015,-42.3079582990257));
#66734=CARTESIAN_POINT('Ctrl Pts',(-25.3492266853846,27.0496284476332,-42.313809804168));
#66735=CARTESIAN_POINT('Ctrl Pts',(-25.2445626164815,27.0995908272907,-42.3196613093103));
#66736=CARTESIAN_POINT('Ctrl Pts',(-25.1398637909194,27.1495697983669,-42.3255147576101));
#66737=CARTESIAN_POINT('Ctrl Pts',(-25.0329941972818,27.194891934655,-42.3313682059099));
#66738=CARTESIAN_POINT('Ctrl Pts',(-24.924409031352,27.2353825042255,-42.3372216542097));
#66739=CARTESIAN_POINT('Ctrl Pts',(-24.8157003805099,27.2759191203658,-42.3430817591512));
#66740=CARTESIAN_POINT('Ctrl Pts',(-24.7052726508419,27.3116130583335,-42.3489418640928));
#66741=CARTESIAN_POINT('Ctrl Pts',(-24.5935972494911,27.3423391340604,-42.3548019690343));
#66742=CARTESIAN_POINT('Ctrl Pts',(-24.4818466417466,27.3730859018763,-42.3606660203898));
#66743=CARTESIAN_POINT('Ctrl Pts',(-24.3688470913055,27.3988580541119,-42.3665300717453));
#66744=CARTESIAN_POINT('Ctrl Pts',(-24.2550795539619,27.4195816555452,-42.3723941231008));
#66745=CARTESIAN_POINT('Ctrl Pts',(-24.1411443459788,27.44033579943,-42.3782668168973));
#66746=CARTESIAN_POINT('Ctrl Pts',(-24.0264393001511,27.4560264867828,-42.3841395106939));
#66747=CARTESIAN_POINT('Ctrl Pts',(-23.9114499219983,27.4666316559922,-42.3900122044905));
#66748=CARTESIAN_POINT('Ctrl Pts',(-23.8799677537996,27.4695351739188,-42.3916200498137));
#66749=CARTESIAN_POINT('Ctrl Pts',(-23.8484642667136,27.4720577966671,-42.3932278951369));
#66750=CARTESIAN_POINT('Ctrl Pts',(-23.8169493924268,27.4741997515833,-42.3948357404602));
#66751=CARTESIAN_POINT('Ctrl Pts',(-23.7018483325979,27.4820227648919,-42.4007080374289));
#66752=CARTESIAN_POINT('Ctrl Pts',(-23.5862099470765,27.4847902047025,-42.4065803343976));
#66753=CARTESIAN_POINT('Ctrl Pts',(-23.470515815206,27.4824441669078,-42.4124526313663));
#66754=CARTESIAN_POINT('Ctrl Pts',(-23.354971613742,27.4801011693917,-42.4183173183045));
#66755=CARTESIAN_POINT('Ctrl Pts',(-23.2393722190771,27.4726578806235,-42.4241820052427));
#66756=CARTESIAN_POINT('Ctrl Pts',(-23.1242036658475,27.4601082021648,-42.4300466921809));
#66757=CARTESIAN_POINT('Ctrl Pts',(-23.0091535562656,27.4475714302647,-42.4359053476557));
#66758=CARTESIAN_POINT('Ctrl Pts',(-22.8945338152629,27.4299387588919,-42.4417640031305));
#66759=CARTESIAN_POINT('Ctrl Pts',(-22.7808291353859,27.407256114427,-42.4476226586053));
#66760=CARTESIAN_POINT('Ctrl Pts',(-22.6626830505631,27.3836874658906,-42.4537101583232));
#66761=CARTESIAN_POINT('Ctrl Pts',(-22.5455254249626,27.3546662981129,-42.4597976580411));
#66762=CARTESIAN_POINT('Ctrl Pts',(-22.4298930064545,27.3203033979565,-42.465885157759));
#66763=CARTESIAN_POINT('Ctrl Pts',(-22.3187363868413,27.2872705869959,-42.4717370278424));
#66764=CARTESIAN_POINT('Ctrl Pts',(-22.2089895302267,27.2493020094543,-42.4775888979258));
#66765=CARTESIAN_POINT('Ctrl Pts',(-22.1011167025963,27.2065476987759,-42.4834407680092));
#66766=CARTESIAN_POINT('Ctrl Pts',(-21.9932602995848,27.16379989783,-42.4892917470922));
#66767=CARTESIAN_POINT('Ctrl Pts',(-21.8872777424082,27.1162679648508,-42.4951427261752));
#66768=CARTESIAN_POINT('Ctrl Pts',(-21.7836147952294,27.0641506673974,-42.5009937052582));
#66769=CARTESIAN_POINT('Ctrl Pts',(-21.6799425277543,27.0120286840976,-42.5068452104004));
#66770=CARTESIAN_POINT('Ctrl Pts',(-21.5785906542202,26.9553207024679,-42.5126967155427));
#66771=CARTESIAN_POINT('Ctrl Pts',(-21.4799810996665,26.8942718494808,-42.518548220685));
#66772=CARTESIAN_POINT('Ctrl Pts',(-21.3813387990259,26.8332027234983,-42.5244016689848));
#66773=CARTESIAN_POINT('Ctrl Pts',(-21.2854409794558,26.767790077292,-42.5302551172846));
#66774=CARTESIAN_POINT('Ctrl Pts',(-21.1926806984784,26.6983224246965,-42.5361085655844));
#66775=CARTESIAN_POINT('Ctrl Pts',(-21.0998149289194,26.6287757722956,-42.5419686705259));
#66776=CARTESIAN_POINT('Ctrl Pts',(-21.0100941507763,26.5551651571875,-42.5478287754674));
#66777=CARTESIAN_POINT('Ctrl Pts',(-20.9238784990514,26.4778195148151,-42.553688880409));
#66778=CARTESIAN_POINT('Ctrl Pts',(-20.8376047864811,26.4004217849935,-42.5595529317644));
#66779=CARTESIAN_POINT('Ctrl Pts',(-20.7548411949899,26.3192843081161,-42.5654169831198));
#66780=CARTESIAN_POINT('Ctrl Pts',(-20.6759099045163,26.2347717552402,-42.5712810344753));
#66781=CARTESIAN_POINT('Ctrl Pts',(-20.5968622850767,26.1501346477316,-42.5771537282718));
#66782=CARTESIAN_POINT('Ctrl Pts',(-20.5216585065826,26.062112849817,-42.5830264220684));
#66783=CARTESIAN_POINT('Ctrl Pts',(-20.4505795661531,25.9711029001998,-42.588899115865));
#66784=CARTESIAN_POINT('Ctrl Pts',(-20.4311193412691,25.9461858984053,-42.5905069611883));
#66785=CARTESIAN_POINT('Ctrl Pts',(-20.4119680461269,25.9210450706819,-42.5921148065117));
#66786=CARTESIAN_POINT('Ctrl Pts',(-20.393130857954,25.8956888956146,-42.593722651835));
#66787=CARTESIAN_POINT('Ctrl Pts',(-20.3243322232833,25.8030811131209,-42.5995949488037));
#66788=CARTESIAN_POINT('Ctrl Pts',(-20.2594964801044,25.7072885177101,-42.6054672457724));
#66789=CARTESIAN_POINT('Ctrl Pts',(-20.1989326581651,25.6086849705391,-42.6113395427411));
#66790=CARTESIAN_POINT('Ctrl Pts',(-20.1384473221291,25.5102092057341,-42.6172042296793));
#66791=CARTESIAN_POINT('Ctrl Pts',(-20.0822231124325,25.4089300823247,-42.6230689166175));
#66792=CARTESIAN_POINT('Ctrl Pts',(-20.0305278821194,25.3052532129406,-42.6289336035557));
#66793=CARTESIAN_POINT('Ctrl Pts',(-19.9788858171146,25.2016829687268,-42.6347922590306));
#66794=CARTESIAN_POINT('Ctrl Pts',(-19.9317636502982,25.095720251124,-42.6406509145054));
#66795=CARTESIAN_POINT('Ctrl Pts',(-19.8893847399046,24.9877976652596,-42.6465095699802));
#66796=CARTESIAN_POINT('Ctrl Pts',(-19.845350471944,24.8756595281341,-42.6525970696981));
#66797=CARTESIAN_POINT('Ctrl Pts',(-19.8064378040184,24.7614056805383,-42.658684569416));
#66798=CARTESIAN_POINT('Ctrl Pts',(-19.7728436642594,24.6455475824569,-42.6647720691339));
#66799=CARTESIAN_POINT('Ctrl Pts',(-19.7405498571887,24.5341740186785,-42.6706239392173));
#66800=CARTESIAN_POINT('Ctrl Pts',(-19.7131706300209,24.4213185210852,-42.6764758093007));
#66801=CARTESIAN_POINT('Ctrl Pts',(-19.690830712549,24.3074527838771,-42.6823276793841));
#66802=CARTESIAN_POINT('Ctrl Pts',(-19.6684941965327,24.193604383763,-42.6881786584671));
#66803=CARTESIAN_POINT('Ctrl Pts',(-19.6511955441772,24.0787464554119,-42.6940296375501));
#66804=CARTESIAN_POINT('Ctrl Pts',(-19.6390084834272,23.9633614699852,-42.6998806166331));
#66805=CARTESIAN_POINT('Ctrl Pts',(-19.6268203269432,23.8479661103381,-42.7057321217754));
#66806=CARTESIAN_POINT('Ctrl Pts',(-19.6197447190927,23.732044010534,-42.7115836269177));
#66807=CARTESIAN_POINT('Ctrl Pts',(-19.6178034988114,23.6160826447082,-42.71743513206));
#66808=CARTESIAN_POINT('Ctrl Pts',(-19.6158616338932,23.500082770637,-42.7232885803598));
#66809=CARTESIAN_POINT('Ctrl Pts',(-19.6190575537813,23.3840440177222,-42.7291420286595));
#66810=CARTESIAN_POINT('Ctrl Pts',(-19.6273609911997,23.2684530258104,-42.7349954769593));
#66811=CARTESIAN_POINT('Ctrl Pts',(-19.6356738714294,23.152730581841,-42.7408555819009));
#66812=CARTESIAN_POINT('Ctrl Pts',(-19.6491058328568,23.0374573277903,-42.7467156868424));
#66813=CARTESIAN_POINT('Ctrl Pts',(-19.6675748048108,22.9231140548297,-42.752575791784));
#66814=CARTESIAN_POINT('Ctrl Pts',(-19.6860562144616,22.808693778831,-42.7584398431394));
#66815=CARTESIAN_POINT('Ctrl Pts',(-19.7095813053045,22.695205134767,-42.7643038944949));
#66816=CARTESIAN_POINT('Ctrl Pts',(-19.7380174253758,22.5831162981918,-42.7701679458503));
#66817=CARTESIAN_POINT('Ctrl Pts',(-19.7664954546116,22.4708622650464,-42.7760406396469));
#66818=CARTESIAN_POINT('Ctrl Pts',(-19.7998988396582,22.3600125511299,-42.7819133334435));
#66819=CARTESIAN_POINT('Ctrl Pts',(-19.8380458567064,22.2510179100126,-42.7877860272401));
#66820=CARTESIAN_POINT('Ctrl Pts',(-19.8484898718523,22.221177000533,-42.7893938725634));
#66821=CARTESIAN_POINT('Ctrl Pts',(-19.8592891851295,22.1914750114253,-42.7910017178867));
#66822=CARTESIAN_POINT('Ctrl Pts',(-19.8704394618732,22.1619208814124,-42.79260956321));
#66823=CARTESIAN_POINT('Ctrl Pts',(-19.9111633644607,22.0539810033831,-42.7984818601787));
#66824=CARTESIAN_POINT('Ctrl Pts',(-19.9567088144411,21.9476536460607,-42.8043541571474));
#66825=CARTESIAN_POINT('Ctrl Pts',(-20.0069283198299,21.8434008891616,-42.8102264541161));
#66826=CARTESIAN_POINT('Ctrl Pts',(-20.057082744728,21.7392832355559,-42.8160911410543));
#66827=CARTESIAN_POINT('Ctrl Pts',(-20.1118990016838,21.6372352048653,-42.8219558279925));
#66828=CARTESIAN_POINT('Ctrl Pts',(-20.1711806279119,21.5377013971714,-42.8278205149307));
#66829=CARTESIAN_POINT('Ctrl Pts',(-20.2304012866987,21.4382699537674,-42.8336791704055));
#66830=CARTESIAN_POINT('Ctrl Pts',(-20.2940779700719,21.3413479432545,-42.8395378258803));
#66831=CARTESIAN_POINT('Ctrl Pts',(-20.3619674546744,21.2473571220733,-42.8453964813551));
#66832=CARTESIAN_POINT('Ctrl Pts',(-20.4325087623416,21.1496949366309,-42.851483981073));
#66833=CARTESIAN_POINT('Ctrl Pts',(-20.5075984946643,21.0551980080289,-42.8575714807909));
#66834=CARTESIAN_POINT('Ctrl Pts',(-20.5869127997796,20.9643084810125,-42.8636589805088));
#66835=CARTESIAN_POINT('Ctrl Pts',(-20.6631570758859,20.8769370266079,-42.8695108505922));
#66836=CARTESIAN_POINT('Ctrl Pts',(-20.7433046665563,20.7928992426831,-42.8753627206756));
#66837=CARTESIAN_POINT('Ctrl Pts',(-20.8270261492867,20.7125550372174,-42.881214590759));
#66838=CARTESIAN_POINT('Ctrl Pts',(-20.9107348846602,20.6322230648875,-42.8870655698419));
#66839=CARTESIAN_POINT('Ctrl Pts',(-20.9980161319563,20.555583838973,-42.8929165489249));
#66840=CARTESIAN_POINT('Ctrl Pts',(-21.0885038331717,20.4829601841468,-42.8987675280078));
#66841=CARTESIAN_POINT('Ctrl Pts',(-21.1789996701022,20.4103299997552,-42.9046190331501));
#66842=CARTESIAN_POINT('Ctrl Pts',(-21.2727022116373,20.3417163629236,-42.9104705382924));
#66843=CARTESIAN_POINT('Ctrl Pts',(-21.3692131424786,20.2774011475507,-42.9163220434347));
#66844=CARTESIAN_POINT('Ctrl Pts',(-21.4657561224994,20.2130645744946,-42.9221754917345));
#66845=CARTESIAN_POINT('Ctrl Pts',(-21.5651090024377,20.153029490336,-42.9280289400342));
#66846=CARTESIAN_POINT('Ctrl Pts',(-21.6668460032796,20.0975334801748,-42.933882388334));
#66847=CARTESIAN_POINT('Ctrl Pts',(-21.7686987011828,20.0419743589995,-42.9397424932755));
#66848=CARTESIAN_POINT('Ctrl Pts',(-21.8729405684713,19.9909648129188,-42.9456025982171));
#66849=CARTESIAN_POINT('Ctrl Pts',(-21.979122744789,19.94469568251,-42.9514627031586));
#66850=CARTESIAN_POINT('Ctrl Pts',(-22.0853764281566,19.8983953927378,-42.957326754514));
#66851=CARTESIAN_POINT('Ctrl Pts',(-22.1935726374476,19.8568420231322,-42.9631908058694));
#66852=CARTESIAN_POINT('Ctrl Pts',(-22.3032457847031,19.8201770401044,-42.9690548572249));
#66853=CARTESIAN_POINT('Ctrl Pts',(-22.413080568285,19.7834580202107,-42.9749275510214));
#66854=CARTESIAN_POINT('Ctrl Pts',(-22.5243962381538,19.7516418788758,-42.980800244818));
#66855=CARTESIAN_POINT('Ctrl Pts',(-22.6367153383455,19.7248193802238,-42.9866729386145));
#66856=CARTESIAN_POINT('Ctrl Pts',(-22.6674664291102,19.7174758287782,-42.9882807839379));
#66857=CARTESIAN_POINT('Ctrl Pts',(-22.6982926975374,19.710506287962,-42.9898886292613));
#66858=CARTESIAN_POINT('Ctrl Pts',(-22.7291842802592,19.7039119427076,-42.9914964745847));
#66859=CARTESIAN_POINT('Ctrl Pts',(-22.8420089064447,19.6798275652591,-42.9973687715534));
#66860=CARTESIAN_POINT('Ctrl Pts',(-22.95608314267,19.660671272331,-43.0032410685221));
#66861=CARTESIAN_POINT('Ctrl Pts',(-23.0709385078465,19.6465687501178,-43.0091133654908));
#66862=CARTESIAN_POINT('Ctrl Pts',(-23.1856450295913,19.6324845036533,-43.014978052429));
#66863=CARTESIAN_POINT('Ctrl Pts',(-23.3011302607094,19.6234410536395,-43.0208427393672));
#66864=CARTESIAN_POINT('Ctrl Pts',(-23.4169139552282,19.6195134378308,-43.0267074263054));
#66865=CARTESIAN_POINT('Ctrl Pts',(-23.5325785734653,19.615589861329,-43.0325660817803));
#66866=CARTESIAN_POINT('Ctrl Pts',(-23.6485406339005,19.6167716679362,-43.0384247372551));
#66867=CARTESIAN_POINT('Ctrl Pts',(-23.7643138332285,19.6230822069966,-43.0442833927299));
#66868=CARTESIAN_POINT('Ctrl Pts',(-23.8846092356939,19.629639241271,-43.0503708924478));
#66869=CARTESIAN_POINT('Ctrl Pts',(-24.0047002708198,19.6417338970295,-43.0564583921657));
#66870=CARTESIAN_POINT('Ctrl Pts',(-24.1240398991526,19.6593327102451,-43.0625458918836));
#66871=CARTESIAN_POINT('Ctrl Pts',(-24.2387602331429,19.6762503239342,-43.068397761967));
#66872=CARTESIAN_POINT('Ctrl Pts',(-24.3527858012207,19.6982538518754,-43.0742496320504));
#66873=CARTESIAN_POINT('Ctrl Pts',(-24.4656357399355,19.7252606909094,-43.0801015021338));
#66874=CARTESIAN_POINT('Ctrl Pts',(-24.578468496221,19.7522634179067,-43.0859524812168));
#66875=CARTESIAN_POINT('Ctrl Pts',(-24.6901255771332,19.7842678451091,-43.0918034602998));
#66876=CARTESIAN_POINT('Ctrl Pts',(-24.8001375149892,19.8211405021979,-43.0976544393827));
#66877=CARTESIAN_POINT('Ctrl Pts',(-24.910159343977,19.8580164744934,-43.103505944525));
#66878=CARTESIAN_POINT('Ctrl Pts',(-25.0185353438925,19.8997614154054,-43.1093574496673));
#66879=CARTESIAN_POINT('Ctrl Pts',(-25.1248130631909,19.946192580382,-43.1152089548096));
#66880=CARTESIAN_POINT('Ctrl Pts',(-25.2311260750058,19.9926391641374,-43.1210624031094));
#66881=CARTESIAN_POINT('Ctrl Pts',(-25.3353390420653,20.0437749009407,-43.1269158514091));
#66882=CARTESIAN_POINT('Ctrl Pts',(-25.4370219284316,20.099370000582,-43.1327692997088));
#66883=CARTESIAN_POINT('Ctrl Pts',(-25.5388204503202,20.1550283239242,-43.1386294046504));
#66884=CARTESIAN_POINT('Ctrl Pts',(-25.6380827856848,20.2151559337651,-43.1444895095919));
#66885=CARTESIAN_POINT('Ctrl Pts',(-25.7344057490944,20.2794783537784,-43.1503496145335));
#66886=CARTESIAN_POINT('Ctrl Pts',(-25.8307935799914,20.343844090916,-43.1562136658889));
#66887=CARTESIAN_POINT('Ctrl Pts',(-25.9242377649184,20.4124100192913,-43.1620777172444));
#66888=CARTESIAN_POINT('Ctrl Pts',(-26.0143676157806,20.4848609005355,-43.1679417685998));
#66889=CARTESIAN_POINT('Ctrl Pts',(-26.1046303000512,20.5574185599159,-43.1738144623964));
#66890=CARTESIAN_POINT('Ctrl Pts',(-26.1915685921458,20.6338723274852,-43.179687156193));
#66891=CARTESIAN_POINT('Ctrl Pts',(-26.2748480454947,20.7138695733865,-43.1855598499895));
#66892=CARTESIAN_POINT('Ctrl Pts',(-26.2976485667273,20.7357714811245,-43.1871676953129));
#66893=CARTESIAN_POINT('Ctrl Pts',(-26.3201750632556,20.7579388056919,-43.1887755406363));
#66894=CARTESIAN_POINT('Ctrl Pts',(-26.3424212066077,20.7803638893781,-43.1903833859597));
#66895=CARTESIAN_POINT('Ctrl Pts',(-26.4225631173301,20.8611504340963,-43.1961756616958));
#66896=CARTESIAN_POINT('Ctrl Pts',(-26.4993481242919,20.9455716560126,-43.201967937432));
#66897=CARTESIAN_POINT('Ctrl Pts',(-26.5724214610187,21.0333131278496,-43.2077602131682));
#66898=CARTESIAN_POINT('Ctrl Pts',(-26.645378490056,21.1209149453568,-43.213543269588));
#66899=CARTESIAN_POINT('Ctrl Pts',(-26.7146353328247,21.2118261747569,-43.2193263260078));
#66900=CARTESIAN_POINT('Ctrl Pts',(-26.7798732943023,21.3056949517399,-43.2251093824277));
#66901=CARTESIAN_POINT('Ctrl Pts',(-26.8450519405058,21.3994783819078,-43.2308871808111));
#66902=CARTESIAN_POINT('Ctrl Pts',(-26.9062187231756,21.4962136705681,-43.2366649791945));
#66903=CARTESIAN_POINT('Ctrl Pts',(-26.9630947331139,21.595515437298,-43.2424427775779));
#66904=CARTESIAN_POINT('Ctrl Pts',(-27.0199336962467,21.6947525227457,-43.2482168125297));
#66905=CARTESIAN_POINT('Ctrl Pts',(-27.0724872296379,21.7965523962866,-43.2539908474816));
#66906=CARTESIAN_POINT('Ctrl Pts',(-27.1205198455029,21.900500941924,-43.2597648824334));
#66907=CARTESIAN_POINT('Ctrl Pts',(-27.1685335558155,22.0044085735983,-43.2655366447353));
#66908=CARTESIAN_POINT('Ctrl Pts',(-27.2120297080586,22.1104628101103,-43.2713084070372));
#66909=CARTESIAN_POINT('Ctrl Pts',(-27.2508192808952,22.2182259798914,-43.2770801693391));
#66910=CARTESIAN_POINT('Ctrl Pts',(-27.2896177420185,22.3260138426474,-43.2828532541891));
#66911=CARTESIAN_POINT('Ctrl Pts',(-27.3237073141794,22.4355110240529,-43.2886263390392));
#66912=CARTESIAN_POINT('Ctrl Pts',(-27.3529477084147,22.5462613001855,-43.2943994238892));
#66913=CARTESIAN_POINT('Ctrl Pts',(-27.3821901415692,22.6570192988831,-43.3001729112938));
#66914=CARTESIAN_POINT('Ctrl Pts',(-27.4065826235527,22.7690301520469,-43.3059463986984));
#66915=CARTESIAN_POINT('Ctrl Pts',(-27.4260355702733,22.8818253944067,-43.3117198861029));
#66916=CARTESIAN_POINT('Ctrl Pts',(-27.4455074752284,22.9947305634875,-43.3174990001681));
#66917=CARTESIAN_POINT('Ctrl Pts',(-27.4600301634214,23.1084212272737,-43.3232781142332));
#66918=CARTESIAN_POINT('Ctrl Pts',(-27.4695657285762,23.2224216839291,-43.3290572282983));
#66919=CARTESIAN_POINT('Ctrl Pts',(-27.4787943419729,23.3327524429809,-43.3346503115206));
#66920=CARTESIAN_POINT('Ctrl Pts',(-27.4833520093356,23.4433729935048,-43.3402433947428));
#66921=CARTESIAN_POINT('Ctrl Pts',(-27.4832508841044,23.5538525231951,-43.3458364779651));
#66922=CARTESIAN_POINT('',(-27.4847506190423,23.5486795567491,-44.5958364779651));
#66923=CARTESIAN_POINT('Ctrl Pts',(-27.4838230626506,23.5538530469273,-43.3458364779651));
#66924=CARTESIAN_POINT('Ctrl Pts',(-27.4864830348576,23.8398784059976,-43.3603144177549));
#66925=CARTESIAN_POINT('Ctrl Pts',(-27.3272802131915,25.4327001523438,-43.4410879946694));
#66926=CARTESIAN_POINT('Ctrl Pts',(-25.1574527633787,27.9157603197276,-43.5881572087097));
#66927=CARTESIAN_POINT('Ctrl Pts',(-20.7462374433328,27.2621590790564,-43.7870441200843));
#66928=CARTESIAN_POINT('Ctrl Pts',(-18.9116742482175,23.1976304391361,-43.9859310314592));
#66929=CARTESIAN_POINT('Ctrl Pts',(-21.3395712090345,19.4571316048511,-44.1848179428342));
#66930=CARTESIAN_POINT('Ctrl Pts',(-25.79889687051,19.477863862913,-44.3837048542089));
#66931=CARTESIAN_POINT('Ctrl Pts',(-27.4473585497634,22.0700013317081,-44.5207110325861));
#66932=CARTESIAN_POINT('Ctrl Pts',(-27.4894342879407,23.4617547981006,-44.591421573838));
#66933=CARTESIAN_POINT('Ctrl Pts',(-27.4889934183657,23.5486778605183,-44.5958364779651));
#66934=CARTESIAN_POINT('',(-27.482494567136,23.5474154798039,-45.8458364377547));
#66935=CARTESIAN_POINT('Ctrl Pts',(-27.4832522173837,23.5486801557959,-44.5958364779651));
#66936=CARTESIAN_POINT('Ctrl Pts',(-27.4832979178416,23.6629911717324,-44.6016509300033));
#66937=CARTESIAN_POINT('Ctrl Pts',(-27.4783557921311,23.7775058598441,-44.6074653820416));
#66938=CARTESIAN_POINT('Ctrl Pts',(-27.4683987986737,23.8917475251493,-44.6132798340798));
#66939=CARTESIAN_POINT('Ctrl Pts',(-27.4584541714557,24.0058473062807,-44.6190870647709));
#66940=CARTESIAN_POINT('Ctrl Pts',(-27.4435070938817,24.1196743220027,-44.624894295462));
#66941=CARTESIAN_POINT('Ctrl Pts',(-27.4235825224486,24.2327507241623,-44.6307015261531));
#66942=CARTESIAN_POINT('Ctrl Pts',(-27.4036771122677,24.3457183819277,-44.6365031720911));
#66943=CARTESIAN_POINT('Ctrl Pts',(-27.3788037988945,24.4579364480779,-44.6423048180292));
#66944=CARTESIAN_POINT('Ctrl Pts',(-27.3490393736304,24.5689318382143,-44.6481064639672));
#66945=CARTESIAN_POINT('Ctrl Pts',(-27.319293827833,24.6798568243785,-44.6539044299423));
#66946=CARTESIAN_POINT('Ctrl Pts',(-27.2846634470628,24.7895602698918,-44.6597023959174));
#66947=CARTESIAN_POINT('Ctrl Pts',(-27.245276028477,24.8975796479591,-44.6655003618925));
#66948=CARTESIAN_POINT('Ctrl Pts',(-27.2059012195097,25.0055644443453,-44.6712964716876));
#66949=CARTESIAN_POINT('Ctrl Pts',(-27.1617725435547,25.1118658485073,-44.6770925814827));
#66950=CARTESIAN_POINT('Ctrl Pts',(-27.1130673171308,25.2160375732509,-44.6828886912778));
#66951=CARTESIAN_POINT('Ctrl Pts',(-27.0643653344555,25.3202023601995,-44.6886844150543));
#66952=CARTESIAN_POINT('Ctrl Pts',(-27.011087586258,25.4222373674284,-44.6944801388308));
#66953=CARTESIAN_POINT('Ctrl Pts',(-26.9534587417486,25.5217181012254,-44.7002758626073));
#66954=CARTESIAN_POINT('Ctrl Pts',(-26.895819123162,25.6212174335753,-44.7060726699311));
#66955=CARTESIAN_POINT('Ctrl Pts',(-26.833827003668,25.7181611785204,-44.7118694772548));
#66956=CARTESIAN_POINT('Ctrl Pts',(-26.7677516010664,25.8121518969598,-44.7176662845786));
#66957=CARTESIAN_POINT('Ctrl Pts',(-26.7016069900243,25.906241062791,-44.7234691635717));
#66958=CARTESIAN_POINT('Ctrl Pts',(-26.6313708000516,25.9973706809659,-44.7292720425648));
#66959=CARTESIAN_POINT('Ctrl Pts',(-26.5573539724366,26.0851746064501,-44.7350749215578));
#66960=CARTESIAN_POINT('Ctrl Pts',(-26.483295396102,26.1730280571786,-44.7408810736278));
#66961=CARTESIAN_POINT('Ctrl Pts',(-26.4054522228431,26.2575517709989,-44.7466872256978));
#66962=CARTESIAN_POINT('Ctrl Pts',(-26.3241725384107,26.33841622781,-44.7524933777678));
#66963=CARTESIAN_POINT('Ctrl Pts',(-26.2427648856999,26.4194079991572,-44.7583086711538));
#66964=CARTESIAN_POINT('Ctrl Pts',(-26.1579102299989,26.4967287260163,-44.7641239645399));
#66965=CARTESIAN_POINT('Ctrl Pts',(-26.069990189229,26.5700888082497,-44.7699392579259));
#66966=CARTESIAN_POINT('Ctrl Pts',(-26.0118362765209,26.6186121685794,-44.7737857309369));
#66967=CARTESIAN_POINT('Ctrl Pts',(-25.9523418936925,26.6654035933763,-44.7776322039478));
#66968=CARTESIAN_POINT('Ctrl Pts',(-25.8916239831666,26.7103899853867,-44.7814786769588));
#66969=CARTESIAN_POINT('Ctrl Pts',(-25.798927738864,26.7790693840677,-44.7873509739275));
#66970=CARTESIAN_POINT('Ctrl Pts',(-25.7030517842149,26.8437817959317,-44.7932232708962));
#66971=CARTESIAN_POINT('Ctrl Pts',(-25.604370377764,26.9042186726172,-44.7990955678649));
#66972=CARTESIAN_POINT('Ctrl Pts',(-25.5058168545787,26.9645772279102,-44.8049602548031));
#66973=CARTESIAN_POINT('Ctrl Pts',(-25.4044654588489,27.0206710526877,-44.8108249417413));
#66974=CARTESIAN_POINT('Ctrl Pts',(-25.3007221475745,27.0722328161194,-44.8166896286795));
#66975=CARTESIAN_POINT('Ctrl Pts',(-25.1970855298013,27.1237415515053,-44.8225482841544));
#66976=CARTESIAN_POINT('Ctrl Pts',(-25.091062257378,27.1707273135183,-44.8284069396292));
#66977=CARTESIAN_POINT('Ctrl Pts',(-24.9830852225184,27.2129673008382,-44.834265595104));
#66978=CARTESIAN_POINT('Ctrl Pts',(-24.8708905095722,27.2568572192673,-44.8403530948219));
#66979=CARTESIAN_POINT('Ctrl Pts',(-24.7565866790089,27.2956228191477,-44.8464405945398));
#66980=CARTESIAN_POINT('Ctrl Pts',(-24.6406854438209,27.3290678307199,-44.8525280942577));
#66981=CARTESIAN_POINT('Ctrl Pts',(-24.5292704126494,27.3612182819278,-44.8583799643411));
#66982=CARTESIAN_POINT('Ctrl Pts',(-24.4163797735725,27.3884522501689,-44.8642318344245));
#66983=CARTESIAN_POINT('Ctrl Pts',(-24.3024853809174,27.4106456127871,-44.8700837045079));
#66984=CARTESIAN_POINT('Ctrl Pts',(-24.1886083297191,27.432835596264,-44.8759346835909));
#66985=CARTESIAN_POINT('Ctrl Pts',(-24.0737282344589,27.4499864210675,-44.8817856626739));
#66986=CARTESIAN_POINT('Ctrl Pts',(-23.9583276607807,27.4620249802169,-44.8876366417569));
#66987=CARTESIAN_POINT('Ctrl Pts',(-23.8429167114804,27.4740646217485,-44.8934881468992));
#66988=CARTESIAN_POINT('Ctrl Pts',(-23.7269856019121,27.4809910410066,-44.8993396520415));
#66989=CARTESIAN_POINT('Ctrl Pts',(-23.6110218339123,27.4827830264149,-44.9051911571838));
#66990=CARTESIAN_POINT('Ctrl Pts',(-23.4950195568699,27.4845756069024,-44.9110446054835));
#66991=CARTESIAN_POINT('Ctrl Pts',(-23.3789850129459,27.4812303568041,-44.9168980537833));
#66992=CARTESIAN_POINT('Ctrl Pts',(-23.2634048026322,27.4727781696387,-44.9227515020831));
#66993=CARTESIAN_POINT('Ctrl Pts',(-23.1476931525214,27.4643163705011,-44.9286116070246));
#66994=CARTESIAN_POINT('Ctrl Pts',(-23.032437279817,27.4507360724773,-44.9344717119662));
#66995=CARTESIAN_POINT('Ctrl Pts',(-22.9181178696736,27.4321199649114,-44.9403318169077));
#66996=CARTESIAN_POINT('Ctrl Pts',(-22.8037214725622,27.4134913205621,-44.9461958682632));
#66997=CARTESIAN_POINT('Ctrl Pts',(-22.6902631974396,27.389820198135,-44.9520599196187));
#66998=CARTESIAN_POINT('Ctrl Pts',(-22.5782110487595,27.3612398519898,-44.9579239709741));
#66999=CARTESIAN_POINT('Ctrl Pts',(-22.4659937575806,27.3326173841197,-44.9637966647707));
#67000=CARTESIAN_POINT('Ctrl Pts',(-22.3551871230178,27.2990713717673,-44.9696693585673));
#67001=CARTESIAN_POINT('Ctrl Pts',(-22.2462416644037,27.2607841186758,-44.9755420523638));
#67002=CARTESIAN_POINT('Ctrl Pts',(-22.2164142202711,27.2503017092472,-44.9771498976871));
#67003=CARTESIAN_POINT('Ctrl Pts',(-22.1867261536364,27.2394641807614,-44.9787577430104));
#67004=CARTESIAN_POINT('Ctrl Pts',(-22.1571863976369,27.2282758793828,-44.9803655883337));
#67005=CARTESIAN_POINT('Ctrl Pts',(-22.0492990174886,27.1874131002841,-44.9862378853024));
#67006=CARTESIAN_POINT('Ctrl Pts',(-21.9430303616688,27.1417308529738,-44.9921101822711));
#67007=CARTESIAN_POINT('Ctrl Pts',(-21.8388423197003,27.0913772239753,-44.9979824792398));
#67008=CARTESIAN_POINT('Ctrl Pts',(-21.7347892971598,27.041088849281,-45.003847166178));
#67009=CARTESIAN_POINT('Ctrl Pts',(-21.6328118952361,26.9861413098332,-45.0097118531162));
#67010=CARTESIAN_POINT('Ctrl Pts',(-21.5333544608102,26.9267316404204,-45.0155765400544));
#67011=CARTESIAN_POINT('Ctrl Pts',(-21.4339993121295,26.8673830701335,-45.0214351955292));
#67012=CARTESIAN_POINT('Ctrl Pts',(-21.337159328819,26.8035817083951,-45.027293851004));
#67013=CARTESIAN_POINT('Ctrl Pts',(-21.2432559539608,26.735571321129,-45.0331525064788));
#67014=CARTESIAN_POINT('Ctrl Pts',(-21.1456846305716,26.6649043882335,-45.0392400061967));
#67015=CARTESIAN_POINT('Ctrl Pts',(-21.0512844148706,26.5896931078885,-45.0453275059146));
#67016=CARTESIAN_POINT('Ctrl Pts',(-20.9604970344649,26.5102619006947,-45.0514150056325));
#67017=CARTESIAN_POINT('Ctrl Pts',(-20.873223772869,26.4339052474536,-45.0572668757159));
#67018=CARTESIAN_POINT('Ctrl Pts',(-20.7892892022547,26.3536495730555,-45.0631187457993));
#67019=CARTESIAN_POINT('Ctrl Pts',(-20.7090528063624,26.2698247629052,-45.0689706158827));
#67020=CARTESIAN_POINT('Ctrl Pts',(-20.6288286271908,26.1860127158445,-45.0748215949657));
#67021=CARTESIAN_POINT('Ctrl Pts',(-20.5523017889219,26.0986329120971,-45.0806725740486));
#67022=CARTESIAN_POINT('Ctrl Pts',(-20.4797946448731,26.0080518248136,-45.0865235531316));
#67023=CARTESIAN_POINT('Ctrl Pts',(-20.4072809817341,25.9174625934184,-45.0923750582739));
#67024=CARTESIAN_POINT('Ctrl Pts',(-20.3387879896089,25.8236718290587,-45.0982265634162));
#67025=CARTESIAN_POINT('Ctrl Pts',(-20.2745970295616,25.7270782094527,-45.1040780685585));
#67026=CARTESIAN_POINT('Ctrl Pts',(-20.2103847530942,25.6304525132088,-45.1099315168582));
#67027=CARTESIAN_POINT('Ctrl Pts',(-20.150477578085,25.5310224550563,-45.115784965158));
#67028=CARTESIAN_POINT('Ctrl Pts',(-20.0951125414928,25.4292141194099,-45.1216384134577));
#67029=CARTESIAN_POINT('Ctrl Pts',(-20.0396845428315,25.3272900055784,-45.1274985183993));
#67030=CARTESIAN_POINT('Ctrl Pts',(-19.9888091901727,25.2229825792895,-45.1333586233408));
#67031=CARTESIAN_POINT('Ctrl Pts',(-19.9426767462872,25.1167409461248,-45.1392187282823));
#67032=CARTESIAN_POINT('Ctrl Pts',(-19.8965132350882,25.0104277658695,-45.1450827796378));
#67033=CARTESIAN_POINT('Ctrl Pts',(-19.8550991400046,24.9021781702167,-45.1509468309932));
#67034=CARTESIAN_POINT('Ctrl Pts',(-19.8185753281554,24.7924579287959,-45.1568108823487));
#67035=CARTESIAN_POINT('Ctrl Pts',(-19.7819976874983,24.6825759816416,-45.1626835761452));
#67036=CARTESIAN_POINT('Ctrl Pts',(-19.7503248271257,24.5712194590503,-45.1685562699418));
#67037=CARTESIAN_POINT('Ctrl Pts',(-19.7236468966377,24.458865933397,-45.1744289637384));
#67038=CARTESIAN_POINT('Ctrl Pts',(-19.7163429255371,24.4281054175168,-45.1760368090617));
#67039=CARTESIAN_POINT('Ctrl Pts',(-19.7094130615039,24.397270205359,-45.1776446543851));
#67040=CARTESIAN_POINT('Ctrl Pts',(-19.7028584767764,24.3663701618082,-45.1792524997085));
#67041=CARTESIAN_POINT('Ctrl Pts',(-19.6789193157971,24.2535146343293,-45.1851247966772));
#67042=CARTESIAN_POINT('Ctrl Pts',(-19.6599098434085,24.1394158399071,-45.1909970936459));
#67043=CARTESIAN_POINT('Ctrl Pts',(-19.6459551428019,24.0245424209907,-45.1968693906147));
#67044=CARTESIAN_POINT('Ctrl Pts',(-19.6320185263791,23.9098178689022,-45.2027340775528));
#67045=CARTESIAN_POINT('Ctrl Pts',(-19.6231237043712,23.7943210951986,-45.208598764491));
#67046=CARTESIAN_POINT('Ctrl Pts',(-19.6193450964312,23.6785324420225,-45.2144634514292));
#67047=CARTESIAN_POINT('Ctrl Pts',(-19.6155703745528,23.5628628702274,-45.220322106904));
#67048=CARTESIAN_POINT('Ctrl Pts',(-19.6169014143407,23.4469024267117,-45.2261807623789));
#67049=CARTESIAN_POINT('Ctrl Pts',(-19.6233609392853,23.3311374444271,-45.2320394178537));
#67050=CARTESIAN_POINT('Ctrl Pts',(-19.6300727789637,23.2108505799699,-45.2381269175716));
#67051=CARTESIAN_POINT('Ctrl Pts',(-19.6423219725357,23.0907752091715,-45.2442144172895));
#67052=CARTESIAN_POINT('Ctrl Pts',(-19.6600743520048,22.9714583279669,-45.2503019170074));
#67053=CARTESIAN_POINT('Ctrl Pts',(-19.6771395878385,22.8567598606287,-45.2561537870908));
#67054=CARTESIAN_POINT('Ctrl Pts',(-19.6992898396032,22.7427627038041,-45.2620056571742));
#67055=CARTESIAN_POINT('Ctrl Pts',(-19.7264418853739,22.6299476142415,-45.2678575272576));
#67056=CARTESIAN_POINT('Ctrl Pts',(-19.7535897969987,22.5171497018023,-45.2737085063406));
#67057=CARTESIAN_POINT('Ctrl Pts',(-19.785737891684,22.4055339005623,-45.2795594854235));
#67058=CARTESIAN_POINT('Ctrl Pts',(-19.8227520950531,22.2955695060498,-45.2854104645065));
#67059=CARTESIAN_POINT('Ctrl Pts',(-19.8597696263553,22.1855952246798,-45.2912619696488));
#67060=CARTESIAN_POINT('Ctrl Pts',(-19.9016540041879,22.0772730370034,-45.2971134747911));
#67061=CARTESIAN_POINT('Ctrl Pts',(-19.9482219018805,21.9710551590127,-45.3029649799334));
#67062=CARTESIAN_POINT('Ctrl Pts',(-19.9948052637582,21.8648020083769,-45.3088184282331));
#67063=CARTESIAN_POINT('Ctrl Pts',(-20.0460750722064,21.760654935333,-45.3146718765329));
#67064=CARTESIAN_POINT('Ctrl Pts',(-20.1018009837828,21.6590436797407,-45.3205253248327));
#67065=CARTESIAN_POINT('Ctrl Pts',(-20.1575902678212,21.5573168700864,-45.3263854297742));
#67066=CARTESIAN_POINT('Ctrl Pts',(-20.2178455707824,21.4581319964804,-45.3322455347157));
#67067=CARTESIAN_POINT('Ctrl Pts',(-20.2822918976991,21.36189189079,-45.3381056396573));
#67068=CARTESIAN_POINT('Ctrl Pts',(-20.3467816251835,21.2655869734118,-45.3439696910127));
#67069=CARTESIAN_POINT('Ctrl Pts',(-20.415467752184,21.1722311048856,-45.3498337423682));
#67070=CARTESIAN_POINT('Ctrl Pts',(-20.4880345635459,21.0821945673122,-45.3556977937236));
#67071=CARTESIAN_POINT('Ctrl Pts',(-20.560708323902,20.9920253338553,-45.3615704875202));
#67072=CARTESIAN_POINT('Ctrl Pts',(-20.6372739109862,20.90518550381,-45.3674431813167));
#67073=CARTESIAN_POINT('Ctrl Pts',(-20.7173782648272,20.8220090696618,-45.3733158751133));
#67074=CARTESIAN_POINT('Ctrl Pts',(-20.7393094969274,20.799236753363,-45.3749237204367));
#67075=CARTESIAN_POINT('Ctrl Pts',(-20.7615057929887,20.7767388031124,-45.3765315657601));
#67076=CARTESIAN_POINT('Ctrl Pts',(-20.7839594871627,20.7545215375217,-45.3781394110835));
#67077=CARTESIAN_POINT('Ctrl Pts',(-20.8659666045865,20.6733779228448,-45.3840117080522));
#67078=CARTESIAN_POINT('Ctrl Pts',(-20.9516844090171,20.595709699402,-45.3898840050209));
#67079=CARTESIAN_POINT('Ctrl Pts',(-21.0407862364668,20.5218754228919,-45.3957563019896));
#67080=CARTESIAN_POINT('Ctrl Pts',(-21.1297725950243,20.4481368297405,-45.4016209889278));
#67081=CARTESIAN_POINT('Ctrl Pts',(-21.2221339402012,20.3782225643031,-45.407485675866));
#67082=CARTESIAN_POINT('Ctrl Pts',(-21.317506379071,20.3124548823735,-45.4133503628042));
#67083=CARTESIAN_POINT('Ctrl Pts',(-21.4127807333576,20.2467548383879,-45.419209018279));
#67084=CARTESIAN_POINT('Ctrl Pts',(-21.5110596835321,20.1851931288619,-45.4250676737538));
#67085=CARTESIAN_POINT('Ctrl Pts',(-21.6119463525326,20.1280517550267,-45.4309263292286));
#67086=CARTESIAN_POINT('Ctrl Pts',(-21.7167737436844,20.0686783887998,-45.4370138289465));
#67087=CARTESIAN_POINT('Ctrl Pts',(-21.8244163761972,20.0140780125992,-45.4431013286644));
#67088=CARTESIAN_POINT('Ctrl Pts',(-21.9343955839625,19.9645175548077,-45.4491888283824));
#67089=CARTESIAN_POINT('Ctrl Pts',(-22.0401178123885,19.9168754400298,-45.4550406984658));
#67090=CARTESIAN_POINT('Ctrl Pts',(-22.1479986831924,19.8738905225356,-45.4608925685492));
#67091=CARTESIAN_POINT('Ctrl Pts',(-22.2575887426771,19.8357526557265,-45.4667444386326));
#67092=CARTESIAN_POINT('Ctrl Pts',(-22.3671621160788,19.7976205957544,-45.4725954177156));
#67093=CARTESIAN_POINT('Ctrl Pts',(-22.4784437704118,19.7643342549019,-45.4784463967986));
#67094=CARTESIAN_POINT('Ctrl Pts',(-22.5909664065899,19.7360345082742,-45.4842973758815));
#67095=CARTESIAN_POINT('Ctrl Pts',(-22.7034991596359,19.7077322172268,-45.4901488810238));
#67096=CARTESIAN_POINT('Ctrl Pts',(-22.8172727154081,19.6844175125014,-45.4960003861662));
#67097=CARTESIAN_POINT('Ctrl Pts',(-22.931807521168,19.6661806002085,-45.5018518913085));
#67098=CARTESIAN_POINT('Ctrl Pts',(-23.0463803614432,19.6479376318341,-45.5077053396083));
#67099=CARTESIAN_POINT('Ctrl Pts',(-23.161714546348,19.6347758738111,-45.513558787908));
#67100=CARTESIAN_POINT('Ctrl Pts',(-23.2773240181326,19.6267338269491,-45.5194122362078));
#67101=CARTESIAN_POINT('Ctrl Pts',(-23.3930649629909,19.6186826345334,-45.5252723411494));
#67102=CARTESIAN_POINT('Ctrl Pts',(-23.5090814069584,19.6157628029639,-45.5311324460909));
#67103=CARTESIAN_POINT('Ctrl Pts',(-23.6248857943885,19.6179607220621,-45.5369925510324));
#67104=CARTESIAN_POINT('Ctrl Pts',(-23.7407681688258,19.6201601213213,-45.5428566023879));
#67105=CARTESIAN_POINT('Ctrl Pts',(-23.8564377908205,19.6274841078252,-45.5487206537434));
#67106=CARTESIAN_POINT('Ctrl Pts',(-23.9714124784033,19.6398672182899,-45.5545847050988));
#67107=CARTESIAN_POINT('Ctrl Pts',(-24.0865566157241,19.6522685789875,-45.5604573988954));
#67108=CARTESIAN_POINT('Ctrl Pts',(-24.2010033674262,19.6697438824968,-45.566330092692));
#67109=CARTESIAN_POINT('Ctrl Pts',(-24.3142808961455,19.6921766306376,-45.5722027864886));
#67110=CARTESIAN_POINT('Ctrl Pts',(-24.345294388606,19.6983183418242,-45.5738106318118));
#67111=CARTESIAN_POINT('Ctrl Pts',(-24.3762203306147,19.7048313622488,-45.5754184771351));
#67112=CARTESIAN_POINT('Ctrl Pts',(-24.4070492625013,19.711712657982,-45.5770263224584));
#67113=CARTESIAN_POINT('Ctrl Pts',(-24.5196450704724,19.7368450581514,-45.5828986194271));
#67114=CARTESIAN_POINT('Ctrl Pts',(-24.6313227571216,19.7669779178528,-45.5887709163958));
#67115=CARTESIAN_POINT('Ctrl Pts',(-24.7416040877902,19.8020302237477,-45.5946432133645));
#67116=CARTESIAN_POINT('Ctrl Pts',(-24.851742502613,19.8370371046381,-45.6005079003027));
#67117=CARTESIAN_POINT('Ctrl Pts',(-24.960487769708,19.876950629652,-45.6063725872409));
#67118=CARTESIAN_POINT('Ctrl Pts',(-25.0673720703158,19.9216388424828,-45.6122372741791));
#67119=CARTESIAN_POINT('Ctrl Pts',(-25.1741464471114,19.9662810962841,-45.618095929654));
#67120=CARTESIAN_POINT('Ctrl Pts',(-25.2790632851435,20.0156881122298,-45.6239545851288));
#67121=CARTESIAN_POINT('Ctrl Pts',(-25.3816708031678,20.0696784246089,-45.6298132406036));
#67122=CARTESIAN_POINT('Ctrl Pts',(-25.4882862612215,20.1257776461435,-45.6359007403215));
#67123=CARTESIAN_POINT('Ctrl Pts',(-25.5924078799858,20.1868253809205,-45.6419882400394));
#67124=CARTESIAN_POINT('Ctrl Pts',(-25.69355234881,20.2525632052186,-45.6480757397573));
#67125=CARTESIAN_POINT('Ctrl Pts',(-25.7907818056711,20.3157565070968,-45.6539276098407));
#67126=CARTESIAN_POINT('Ctrl Pts',(-25.8852599220345,20.3832833235902,-45.6597794799241));
#67127=CARTESIAN_POINT('Ctrl Pts',(-25.9765840222712,20.4548681455744,-45.6656313500075));
#67128=CARTESIAN_POINT('Ctrl Pts',(-26.0678942175833,20.5264420681185,-45.6714823290905));
#67129=CARTESIAN_POINT('Ctrl Pts',(-26.1560510263601,20.602072512681,-45.6773333081735));
#67130=CARTESIAN_POINT('Ctrl Pts',(-26.2406833330455,20.6814424816665,-45.6831842872565));
#67131=CARTESIAN_POINT('Ctrl Pts',(-26.3253232489896,20.7608195867758,-45.6890357923987));
#67132=CARTESIAN_POINT('Ctrl Pts',(-26.406437731353,20.8439366018829,-45.694887297541));
#67133=CARTESIAN_POINT('Ctrl Pts',(-26.4836916696365,20.9304388314498,-45.7007388026833));
#67134=CARTESIAN_POINT('Ctrl Pts',(-26.5609712622708,21.0169697865237,-45.7065922509831));
#67135=CARTESIAN_POINT('Ctrl Pts',(-26.6343874864306,21.1068878832111,-45.7124456992828));
#67136=CARTESIAN_POINT('Ctrl Pts',(-26.7036452159199,21.1998050042919,-45.7182991475826));
#67137=CARTESIAN_POINT('Ctrl Pts',(-26.772981706487,21.2928277923163,-45.7241592525241));
#67138=CARTESIAN_POINT('Ctrl Pts',(-26.8381500160266,21.3888560804348,-45.7300193574656));
#67139=CARTESIAN_POINT('Ctrl Pts',(-26.8988980505145,21.4874723230232,-45.7358794624072));
#67140=CARTESIAN_POINT('Ctrl Pts',(-26.9596869950014,21.5861549774786,-45.7417435137626));
#67141=CARTESIAN_POINT('Ctrl Pts',(-27.0160495365432,21.6874286963868,-45.747607565118));
#67142=CARTESIAN_POINT('Ctrl Pts',(-27.0677801107037,21.7908524262868,-45.7534716164735));
#67143=CARTESIAN_POINT('Ctrl Pts',(-27.1195869254044,21.8944285821198,-45.7593443102701));
#67144=CARTESIAN_POINT('Ctrl Pts',(-27.1667479803943,22.0001606969201,-45.7652170040666));
#67145=CARTESIAN_POINT('Ctrl Pts',(-27.2091062394496,22.107588833792,-45.7710896978632));
#67146=CARTESIAN_POINT('Ctrl Pts',(-27.2207032222119,22.1370008606145,-45.7726975431866));
#67147=CARTESIAN_POINT('Ctrl Pts',(-27.2319404915516,22.166539938157,-45.7743053885099));
#67148=CARTESIAN_POINT('Ctrl Pts',(-27.2428154866116,22.1961964678728,-45.7759132338333));
#67149=CARTESIAN_POINT('Ctrl Pts',(-27.288696711522,22.3213163325201,-45.7826966771815));
#67150=CARTESIAN_POINT('Ctrl Pts',(-27.3282525808161,22.448873430684,-45.7894801205297));
#67151=CARTESIAN_POINT('Ctrl Pts',(-27.3612536578878,22.5782651777892,-45.7962635638779));
#67152=CARTESIAN_POINT('Ctrl Pts',(-27.3941183897617,22.7071223379985,-45.8030189811734));
#67153=CARTESIAN_POINT('Ctrl Pts',(-27.420482277308,22.8377988841297,-45.8097743984689));
#67154=CARTESIAN_POINT('Ctrl Pts',(-27.4401653876646,22.9696778397244,-45.8165298157645));
#67155=CARTESIAN_POINT('Ctrl Pts',(-27.4596999042476,23.1005612010595,-45.8232342343646));
#67156=CARTESIAN_POINT('Ctrl Pts',(-27.4726540447025,23.2326287353507,-45.8299386529647));
#67157=CARTESIAN_POINT('Ctrl Pts',(-27.4788993718126,23.365257921968,-45.8366430715649));
#67158=CARTESIAN_POINT('Ctrl Pts',(-27.4817539829892,23.4258800081761,-45.8397075240638));
#67159=CARTESIAN_POINT('Ctrl Pts',(-27.4832076421927,23.4866191808702,-45.8427719765627));
#67160=CARTESIAN_POINT('Ctrl Pts',(-27.4832515079284,23.5474147613741,-45.8458364290615));
#67161=CARTESIAN_POINT('',(-27.4786603534827,23.5529148598696,-47.095836477965));
#67162=CARTESIAN_POINT('Ctrl Pts',(-27.4789932982812,23.5474188029378,-45.845836477965));
#67163=CARTESIAN_POINT('Ctrl Pts',(-27.4733443827607,24.3993354066055,-45.8888243670461));
#67164=CARTESIAN_POINT('Ctrl Pts',(-26.7819451567561,26.5734232824688,-45.998107893252));
#67165=CARTESIAN_POINT('Ctrl Pts',(-23.1916612413879,28.1883731768075,-46.1736870565831));
#67166=CARTESIAN_POINT('Ctrl Pts',(-19.454290019253,25.7556644952009,-46.3725739679577));
#67167=CARTESIAN_POINT('Ctrl Pts',(-19.4807610656983,21.2963692072287,-46.571460879333));
#67168=CARTESIAN_POINT('Ctrl Pts',(-23.2467497334191,18.9082015966501,-46.7703477907076));
#67169=CARTESIAN_POINT('Ctrl Pts',(-26.8015964030055,20.5582290572362,-46.9451396569184));
#67170=CARTESIAN_POINT('Ctrl Pts',(-27.4734779850077,22.7164226323347,-47.0536358860042));
#67171=CARTESIAN_POINT('Ctrl Pts',(-27.4786603534827,23.5529148598696,-47.095836477965));
#67172=CARTESIAN_POINT('',(-27.4887212107966,23.5520805994482,-48.345836477965));
#67173=CARTESIAN_POINT('Ctrl Pts',(-27.4786603534827,23.5529148598696,-47.095836477965));
#67174=CARTESIAN_POINT('Ctrl Pts',(-27.4816193025558,24.0305223308889,-47.1199315231292));
#67175=CARTESIAN_POINT('Ctrl Pts',(-27.1794543469686,25.8186135203327,-47.2103222054181));
#67176=CARTESIAN_POINT('Ctrl Pts',(-24.5097012594312,28.1021981564742,-47.3670085248325));
#67177=CARTESIAN_POINT('Ctrl Pts',(-20.2392470151605,26.817972425073,-47.5658954362071));
#67178=CARTESIAN_POINT('Ctrl Pts',(-19.0113261136081,22.530989168614,-47.7647823475823));
#67179=CARTESIAN_POINT('Ctrl Pts',(-21.9542937527826,19.1806225235446,-47.963669258957));
#67180=CARTESIAN_POINT('Ctrl Pts',(-26.2484742764648,19.8281824805853,-48.1573539690847));
#67181=CARTESIAN_POINT('Ctrl Pts',(-27.4817984742678,22.3490190787578,-48.2847430420873));
#67182=CARTESIAN_POINT('Ctrl Pts',(-27.4887212107966,23.5520805994482,-48.345836477965));
#67183=CARTESIAN_POINT('',(-27.4832509287299,23.5467016283086,-49.595836477965));
#67184=CARTESIAN_POINT('Ctrl Pts',(-27.4887212107966,23.5520805994482,-48.345836477965));
#67185=CARTESIAN_POINT('Ctrl Pts',(-27.4893106925975,23.6545231622795,-48.3510386792123));
#67186=CARTESIAN_POINT('Ctrl Pts',(-27.4856616780405,23.7569230546521,-48.3562408804595));
#67187=CARTESIAN_POINT('Ctrl Pts',(-27.3754023991223,25.1595582326159,-48.4277387188318));
#67188=CARTESIAN_POINT('Ctrl Pts',(-25.7503914835099,27.6490498461281,-48.5603299930818));
#67189=CARTESIAN_POINT('Ctrl Pts',(-21.2911339543954,27.6168400551349,-48.7592169044564));
#67190=CARTESIAN_POINT('Ctrl Pts',(-18.9078148561469,23.8477811198626,-48.9581038158317));
#67191=CARTESIAN_POINT('Ctrl Pts',(-20.7905023679254,19.8053186383279,-49.1569907272063));
#67192=CARTESIAN_POINT('Ctrl Pts',(-25.2091662919772,19.204132886764,-49.3558776385813));
#67193=CARTESIAN_POINT('Ctrl Pts',(-27.337905242507,21.6993486153379,-49.5021595555008));
#67194=CARTESIAN_POINT('Ctrl Pts',(-27.4868110529832,23.2763131213276,-49.5821458352954));
#67195=CARTESIAN_POINT('Ctrl Pts',(-27.4842993531624,23.5467006817397,-49.595836477965));
#67196=CARTESIAN_POINT('',(-27.4832525273076,23.5500667762137,-50.845836477928));
#67197=CARTESIAN_POINT('Ctrl Pts',(-27.4832509287299,23.5467016283086,-49.595836477965));
#67198=CARTESIAN_POINT('Ctrl Pts',(-27.483353921989,23.6607774786029,-49.6016141195103));
#67199=CARTESIAN_POINT('Ctrl Pts',(-27.478489605921,23.7750111715627,-49.6073917610556));
#67200=CARTESIAN_POINT('Ctrl Pts',(-27.4686435306552,23.8889278618572,-49.6131694026009));
#67201=CARTESIAN_POINT('Ctrl Pts',(-27.4586683176372,24.0043386444607,-49.6190228217147));
#67202=CARTESIAN_POINT('Ctrl Pts',(-27.4435796743107,24.1194236090951,-49.6248762408284));
#67203=CARTESIAN_POINT('Ctrl Pts',(-27.4234171929912,24.2336883417597,-49.6307296599422));
#67204=CARTESIAN_POINT('Ctrl Pts',(-27.4035424495562,24.3463224074482,-49.6364995451691));
#67205=CARTESIAN_POINT('Ctrl Pts',(-27.3787378179568,24.4581590660768,-49.642269430396));
#67206=CARTESIAN_POINT('Ctrl Pts',(-27.3490933288047,24.5687306110897,-49.648039315623));
#67207=CARTESIAN_POINT('Ctrl Pts',(-27.3194550330856,24.6792790550987,-49.6538079953848));
#67208=CARTESIAN_POINT('Ctrl Pts',(-27.284978999474,24.7885624992263,-49.6595766751466));
#67209=CARTESIAN_POINT('Ctrl Pts',(-27.2458058797152,24.8961256505024,-49.6653453549084));
#67210=CARTESIAN_POINT('Ctrl Pts',(-27.2066308287074,25.0036941046812,-49.6711143190682));
#67211=CARTESIAN_POINT('Ctrl Pts',(-27.1627583780813,25.1095416972608,-49.676883283228));
#67212=CARTESIAN_POINT('Ctrl Pts',(-27.1143780351475,25.2132313035472,-49.6826522473879));
#67213=CARTESIAN_POINT('Ctrl Pts',(-27.0647595620063,25.319574492383,-49.6885688485498));
#67214=CARTESIAN_POINT('Ctrl Pts',(-27.0103995267252,25.4236473098046,-49.6944854497117));
#67215=CARTESIAN_POINT('Ctrl Pts',(-26.9515528064239,25.525004526534,-49.7004020508737));
#67216=CARTESIAN_POINT('Ctrl Pts',(-26.8940929348259,25.6239730438783,-49.706179214687));
#67217=CARTESIAN_POINT('Ctrl Pts',(-26.8323557985413,25.7203522122916,-49.7119563785004));
#67218=CARTESIAN_POINT('Ctrl Pts',(-26.766622182131,25.8137576171201,-49.7177335423138));
#67219=CARTESIAN_POINT('Ctrl Pts',(-26.698508750604,25.9105446645012,-49.72371986215));
#67220=CARTESIAN_POINT('Ctrl Pts',(-26.6261043021226,26.0041381491129,-49.7297061819862));
#67221=CARTESIAN_POINT('Ctrl Pts',(-26.5497651972763,26.0941496933366,-49.7356925018224));
#67222=CARTESIAN_POINT('Ctrl Pts',(-26.4734260924301,26.1841612375603,-49.7416788216586));
#67223=CARTESIAN_POINT('Ctrl Pts',(-26.3931527277981,26.2705905268623,-49.7476651414949));
#67224=CARTESIAN_POINT('Ctrl Pts',(-26.309340642267,26.3530942678784,-49.7536514613311));
#67225=CARTESIAN_POINT('Ctrl Pts',(-26.2271249456003,26.4340265403813,-49.7595237582998));
#67226=CARTESIAN_POINT('Ctrl Pts',(-26.1412075193273,26.5114738824381,-49.7653960552685));
#67227=CARTESIAN_POINT('Ctrl Pts',(-26.0519159492196,26.5850785803196,-49.7712683522372));
#67228=CARTESIAN_POINT('Ctrl Pts',(-25.9627400938953,26.6585878923582,-49.7771330391753));
#67229=CARTESIAN_POINT('Ctrl Pts',(-25.8701991063477,26.7282642026664,-49.7829977261135));
#67230=CARTESIAN_POINT('Ctrl Pts',(-25.7746577077335,26.7937861931211,-49.7888624130517));
#67231=CARTESIAN_POINT('Ctrl Pts',(-25.6792145674669,26.8592407983103,-49.7947210685265));
#67232=CARTESIAN_POINT('Ctrl Pts',(-25.5807774926853,26.9205493493911,-49.8005797240013));
#67233=CARTESIAN_POINT('Ctrl Pts',(-25.4797440849629,26.9774308675654,-49.8064383794761));
#67234=CARTESIAN_POINT('Ctrl Pts',(-25.3747642233455,27.0365342279403,-49.812525879194));
#67235=CARTESIAN_POINT('Ctrl Pts',(-25.2669814146164,27.090857368111,-49.8186133789119));
#67236=CARTESIAN_POINT('Ctrl Pts',(-25.1568750103301,27.14013459259,-49.8247008786299));
#67237=CARTESIAN_POINT('Ctrl Pts',(-25.0510305087958,27.1875044372034,-49.8305527487132));
#67238=CARTESIAN_POINT('Ctrl Pts',(-24.9430393589257,27.2302115439541,-49.8364046187966));
#67239=CARTESIAN_POINT('Ctrl Pts',(-24.8333515015809,27.2680672168924,-49.84225648888));
#67240=CARTESIAN_POINT('Ctrl Pts',(-24.7236803452098,27.3059171259603,-49.848107467963));
#67241=CARTESIAN_POINT('Ctrl Pts',(-24.6123133856832,27.3389169351134,-49.8539584470459));
#67242=CARTESIAN_POINT('Ctrl Pts',(-24.4997182831299,27.3669269724673,-49.8598094261289));
#67243=CARTESIAN_POINT('Ctrl Pts',(-24.3871130571933,27.3949395281931,-49.8656609312712));
#67244=CARTESIAN_POINT('Ctrl Pts',(-24.2732798699017,27.417961320487,-49.8715124364135));
#67245=CARTESIAN_POINT('Ctrl Pts',(-24.1586985045816,27.4359033778302,-49.8773639415558));
#67246=CARTESIAN_POINT('Ctrl Pts',(-24.0440790892849,27.4538513933399,-49.8832173898555));
#67247=CARTESIAN_POINT('Ctrl Pts',(-23.9287114101153,27.4667162557479,-49.8890708381553));
#67248=CARTESIAN_POINT('Ctrl Pts',(-23.8130816223074,27.4744607154081,-49.894924286455));
#67249=CARTESIAN_POINT('Ctrl Pts',(-23.6973203383219,27.4822139822008,-49.9007843913965));
#67250=CARTESIAN_POINT('Ctrl Pts',(-23.5812967634541,27.4848351960527,-49.9066444963381));
#67251=CARTESIAN_POINT('Ctrl Pts',(-23.465498416705,27.4823392219889,-49.9125046012796));
#67252=CARTESIAN_POINT('Ctrl Pts',(-23.3496220870172,27.4798415670427,-49.918368652635));
#67253=CARTESIAN_POINT('Ctrl Pts',(-23.2339716989474,27.4722198894174,-49.9242327039905));
#67254=CARTESIAN_POINT('Ctrl Pts',(-23.1190292643755,27.4595408932407,-49.9300967553459));
#67255=CARTESIAN_POINT('Ctrl Pts',(-23.0039174275996,27.4468432107546,-49.9359694491424));
#67256=CARTESIAN_POINT('Ctrl Pts',(-22.8895160336619,27.4290733972241,-49.941842142939));
#67257=CARTESIAN_POINT('Ctrl Pts',(-22.7762966185154,27.4063491648785,-49.9477148367355));
#67258=CARTESIAN_POINT('Ctrl Pts',(-22.7452990365751,27.4001276501918,-49.949322682059));
#67259=CARTESIAN_POINT('Ctrl Pts',(-22.7143899604881,27.393535052838,-49.9509305273825));
#67260=CARTESIAN_POINT('Ctrl Pts',(-22.6835788420845,27.3865744310841,-49.952538372706));
#67261=CARTESIAN_POINT('Ctrl Pts',(-22.5710480939066,27.3611523102935,-49.9584106696747));
#67262=CARTESIAN_POINT('Ctrl Pts',(-22.4594483344045,27.3307321096337,-49.9642829666434));
#67263=CARTESIAN_POINT('Ctrl Pts',(-22.3492575881372,27.2953960730756,-49.9701552636121));
#67264=CARTESIAN_POINT('Ctrl Pts',(-22.2392096403258,27.2601058292144,-49.9760199505503));
#67265=CARTESIAN_POINT('Ctrl Pts',(-22.1305674645564,27.219912543225,-49.9818846374885));
#67266=CARTESIAN_POINT('Ctrl Pts',(-22.0237985384041,27.1749493750687,-49.9877493244267));
#67267=CARTESIAN_POINT('Ctrl Pts',(-21.9171394174088,27.1300324487161,-49.9936079799015));
#67268=CARTESIAN_POINT('Ctrl Pts',(-21.8123500927711,27.0803555570138,-49.9994666353763));
#67269=CARTESIAN_POINT('Ctrl Pts',(-21.7098818771748,27.0261013278854,-50.0053252908511));
#67270=CARTESIAN_POINT('Ctrl Pts',(-21.6034111628242,26.9697278807805,-50.011412790569));
#67271=CARTESIAN_POINT('Ctrl Pts',(-21.4994470161958,26.9084123555737,-50.017500290287));
#67272=CARTESIAN_POINT('Ctrl Pts',(-21.3984720811977,26.842414419096,-50.0235877900049));
#67273=CARTESIAN_POINT('Ctrl Pts',(-21.301405595995,26.7789710732336,-50.0294396600883));
#67274=CARTESIAN_POINT('Ctrl Pts',(-21.2071015959606,26.711201308627,-50.0352915301717));
#67275=CARTESIAN_POINT('Ctrl Pts',(-21.1159620462723,26.6393816699117,-50.0411434002551));
#67276=CARTESIAN_POINT('Ctrl Pts',(-21.0248363734094,26.5675729663895,-50.046994379338));
#67277=CARTESIAN_POINT('Ctrl Pts',(-20.9368745174852,26.4917158706057,-50.052845358421));
#67278=CARTESIAN_POINT('Ctrl Pts',(-20.8524467769247,26.4121283342986,-50.0586963375039));
#67279=CARTESIAN_POINT('Ctrl Pts',(-20.7680114454979,26.3325336423061,-50.0645478426462));
#67280=CARTESIAN_POINT('Ctrl Pts',(-20.6871111619133,26.2492081266141,-50.0703993477885));
#67281=CARTESIAN_POINT('Ctrl Pts',(-20.6100801226299,26.1625073441076,-50.0762508529308));
#67282=CARTESIAN_POINT('Ctrl Pts',(-20.5330235030151,26.0757777701585,-50.0821043012306));
#67283=CARTESIAN_POINT('Ctrl Pts',(-20.4598389570468,25.9856710095167,-50.0879577495303));
#67284=CARTESIAN_POINT('Ctrl Pts',(-20.3908206109911,25.8925759377256,-50.0938111978301));
#67285=CARTESIAN_POINT('Ctrl Pts',(-20.3217237760889,25.7993749966227,-50.0996713027717));
#67286=CARTESIAN_POINT('Ctrl Pts',(-20.2568028440914,25.7031792936221,-50.1055314077132));
#67287=CARTESIAN_POINT('Ctrl Pts',(-20.1963088334912,25.6044070218152,-50.1113915126547));
#67288=CARTESIAN_POINT('Ctrl Pts',(-20.1357740839611,25.5055682330654,-50.1172555640102));
#67289=CARTESIAN_POINT('Ctrl Pts',(-20.079672391706,25.4041497813089,-50.1231196153656));
#67290=CARTESIAN_POINT('Ctrl Pts',(-20.028208185279,25.3005932476364,-50.128983666721));
#67291=CARTESIAN_POINT('Ctrl Pts',(-19.9766681308849,25.1968840923049,-50.1348563605176));
#67292=CARTESIAN_POINT('Ctrl Pts',(-19.9297793699119,25.0910309426008,-50.1407290543142));
#67293=CARTESIAN_POINT('Ctrl Pts',(-19.8876977542586,24.9834941380829,-50.1466017481107));
#67294=CARTESIAN_POINT('Ctrl Pts',(-19.8761765118319,24.9540523598762,-50.1482095934341));
#67295=CARTESIAN_POINT('Ctrl Pts',(-19.8650153086448,24.924484457216,-50.1498174387575));
#67296=CARTESIAN_POINT('Ctrl Pts',(-19.8542166808408,24.8948000352085,-50.1514252840809));
#67297=CARTESIAN_POINT('Ctrl Pts',(-19.8147770976934,24.7863842946901,-50.1572975810496));
#67298=CARTESIAN_POINT('Ctrl Pts',(-19.7800457218456,24.6760501365121,-50.1631698780183));
#67299=CARTESIAN_POINT('Ctrl Pts',(-19.7502117526039,24.5642441871091,-50.169042174987));
#67300=CARTESIAN_POINT('Ctrl Pts',(-19.720416445817,24.4525831293368,-50.1749068619252));
#67301=CARTESIAN_POINT('Ctrl Pts',(-19.6955060300206,24.3394544690448,-50.1807715488634));
#67302=CARTESIAN_POINT('Ctrl Pts',(-19.6756211669524,24.2253234815646,-50.1866362358017));
#67303=CARTESIAN_POINT('Ctrl Pts',(-19.6557567542211,24.1113098706608,-50.1924948912765));
#67304=CARTESIAN_POINT('Ctrl Pts',(-19.6409076843999,23.9962963877439,-50.1983535467513));
#67305=CARTESIAN_POINT('Ctrl Pts',(-19.6311642631908,23.8807614478816,-50.2042122022261));
#67306=CARTESIAN_POINT('Ctrl Pts',(-19.6210402553674,23.7607136115064,-50.210299701944));
#67307=CARTESIAN_POINT('Ctrl Pts',(-19.6164290068854,23.6401031898881,-50.2163872016619));
#67308=CARTESIAN_POINT('Ctrl Pts',(-19.617372945176,23.5194766003745,-50.2224747013798));
#67309=CARTESIAN_POINT('Ctrl Pts',(-19.6182803463258,23.4035191197751,-50.2283265714632));
#67310=CARTESIAN_POINT('Ctrl Pts',(-19.6243208764983,23.2875471515561,-50.2341784415466));
#67311=CARTESIAN_POINT('Ctrl Pts',(-19.635479153271,23.1720483598653,-50.24003031163));
#67312=CARTESIAN_POINT('Ctrl Pts',(-19.6466357310945,23.0565671539158,-50.245881290713));
#67313=CARTESIAN_POINT('Ctrl Pts',(-19.6629084664319,22.9415593925992,-50.251732269796));
#67314=CARTESIAN_POINT('Ctrl Pts',(-19.6842300231476,22.8275084805869,-50.257583248879));
#67315=CARTESIAN_POINT('Ctrl Pts',(-19.7055534968766,22.7134473142993,-50.2634347540213));
#67316=CARTESIAN_POINT('Ctrl Pts',(-19.7319266184007,22.600343574703,-50.2692862591636));
#67317=CARTESIAN_POINT('Ctrl Pts',(-19.7632308991008,22.4886706204554,-50.275137764306));
#67318=CARTESIAN_POINT('Ctrl Pts',(-19.7945455752707,22.3769605820517,-50.2809912126057));
#67319=CARTESIAN_POINT('Ctrl Pts',(-19.8307945552232,22.266682671597,-50.2868446609055));
#67320=CARTESIAN_POINT('Ctrl Pts',(-19.8718096591547,22.1582945461705,-50.2926981092052));
#67321=CARTESIAN_POINT('Ctrl Pts',(-19.9128714061658,22.0497831599088,-50.2985582141468));
#67322=CARTESIAN_POINT('Ctrl Pts',(-19.9587099491574,21.9431662350625,-50.3044183190883));
#67323=CARTESIAN_POINT('Ctrl Pts',(-20.0091091414018,21.8388810087955,-50.3102784240299));
#67324=CARTESIAN_POINT('Ctrl Pts',(-20.0595422743478,21.7345255529556,-50.3161424753854));
#67325=CARTESIAN_POINT('Ctrl Pts',(-20.1145419764513,21.6325052853654,-50.3220065267408));
#67326=CARTESIAN_POINT('Ctrl Pts',(-20.1738472404311,21.5332308884959,-50.3278705780963));
#67327=CARTESIAN_POINT('Ctrl Pts',(-20.2332399085315,21.4338101809826,-50.3337432718928));
#67328=CARTESIAN_POINT('Ctrl Pts',(-20.2969505763465,21.3371437648161,-50.3396159656894));
#67329=CARTESIAN_POINT('Ctrl Pts',(-20.3646761970398,21.2436115938606,-50.345488659486));
#67330=CARTESIAN_POINT('Ctrl Pts',(-20.3832183390734,21.2180040500564,-50.3470965048093));
#67331=CARTESIAN_POINT('Ctrl Pts',(-20.4020612081979,21.1926312376915,-50.3487043501325));
#67332=CARTESIAN_POINT('Ctrl Pts',(-20.4211980943696,21.1675004824328,-50.3503121954558));
#67333=CARTESIAN_POINT('Ctrl Pts',(-20.4910913092399,21.0757159955843,-50.3561844924245));
#67334=CARTESIAN_POINT('Ctrl Pts',(-20.5651435067155,20.9868556164598,-50.3620567893932));
#67335=CARTESIAN_POINT('Ctrl Pts',(-20.6430812027292,20.9013199421322,-50.3679290863619));
#67336=CARTESIAN_POINT('Ctrl Pts',(-20.7209178976786,20.8158951152453,-50.3737937733001));
#67337=CARTESIAN_POINT('Ctrl Pts',(-20.8026298019172,20.7337867277308,-50.3796584602383));
#67338=CARTESIAN_POINT('Ctrl Pts',(-20.8879015051344,20.6553646217094,-50.3855231471765));
#67339=CARTESIAN_POINT('Ctrl Pts',(-20.9730855117428,20.5770231679149,-50.3913818026513));
#67340=CARTESIAN_POINT('Ctrl Pts',(-21.0618217329104,20.5023607330488,-50.3972404581262));
#67341=CARTESIAN_POINT('Ctrl Pts',(-21.1537564840738,20.4317118964387,-50.403099113601));
#67342=CARTESIAN_POINT('Ctrl Pts',(-21.2492822875929,20.3583034540438,-50.4091866133189));
#67343=CARTESIAN_POINT('Ctrl Pts',(-21.3482612836426,20.2892288874038,-50.4152741130368));
#67344=CARTESIAN_POINT('Ctrl Pts',(-21.4502566959656,20.2248192531691,-50.4213616127547));
#67345=CARTESIAN_POINT('Ctrl Pts',(-21.5483041587459,20.1629027309306,-50.4272134828381));
#67346=CARTESIAN_POINT('Ctrl Pts',(-21.6491384840492,20.1052969650911,-50.4330653529215));
#67347=CARTESIAN_POINT('Ctrl Pts',(-21.7523410769943,20.0522526173061,-50.4389172230049));
#67348=CARTESIAN_POINT('Ctrl Pts',(-21.8555279564064,19.9992163460053,-50.4447682020879));
#67349=CARTESIAN_POINT('Ctrl Pts',(-21.9610820189306,19.9507403007559,-50.4506191811708));
#67350=CARTESIAN_POINT('Ctrl Pts',(-22.0685601700707,19.9070291312552,-50.4564701602538));
#67351=CARTESIAN_POINT('Ctrl Pts',(-22.1760479845304,19.8633140316998,-50.462321665396));
#67352=CARTESIAN_POINT('Ctrl Pts',(-22.2854598485538,19.8243648152735,-50.4681731705383));
#67353=CARTESIAN_POINT('Ctrl Pts',(-22.3963334694385,19.7903376659342,-50.4740246756806));
#67354=CARTESIAN_POINT('Ctrl Pts',(-22.5072439090401,19.7562992169191,-50.4798781239804));
#67355=CARTESIAN_POINT('Ctrl Pts',(-22.619616675744,19.7271862063339,-50.4857315722802));
#67356=CARTESIAN_POINT('Ctrl Pts',(-22.7329758266575,19.703104524741,-50.49158502058));
#67357=CARTESIAN_POINT('Ctrl Pts',(-22.8464638915404,19.678995457047,-50.4974451255215));
#67358=CARTESIAN_POINT('Ctrl Pts',(-22.960940174979,19.6599292246644,-50.503305230463));
#67359=CARTESIAN_POINT('Ctrl Pts',(-23.0759199855418,19.6459603249478,-50.5091653354046));
#67360=CARTESIAN_POINT('Ctrl Pts',(-23.1909772278111,19.6319820180515,-50.51502938676));
#67361=CARTESIAN_POINT('Ctrl Pts',(-23.3065382612459,19.6231079106509,-50.5208934381155));
#67362=CARTESIAN_POINT('Ctrl Pts',(-23.4221164862923,19.619340404227,-50.526757489471));
#67363=CARTESIAN_POINT('Ctrl Pts',(-23.5378650505702,19.6155673452507,-50.5326301832675));
#67364=CARTESIAN_POINT('Ctrl Pts',(-23.6536304452246,19.6169159031184,-50.538502877064));
#67365=CARTESIAN_POINT('Ctrl Pts',(-23.7689291990324,19.6233365006131,-50.5443755708606));
#67366=CARTESIAN_POINT('Ctrl Pts',(-23.8004960691129,19.6250943528037,-50.545983416184));
#67367=CARTESIAN_POINT('Ctrl Pts',(-23.8320280114364,19.6272320940354,-50.5475912615073));
#67368=CARTESIAN_POINT('Ctrl Pts',(-23.8635152357334,19.6297480388696,-50.5491991068306));
#67369=CARTESIAN_POINT('Ctrl Pts',(-23.9785153101229,19.6389369670634,-50.5550714037994));
#67370=CARTESIAN_POINT('Ctrl Pts',(-24.0933033900328,19.65320552129,-50.5609437007681));
#67371=CARTESIAN_POINT('Ctrl Pts',(-24.2073946166921,19.6725401545155,-50.5668159977368));
#67372=CARTESIAN_POINT('Ctrl Pts',(-24.3213379901826,19.6918497315919,-50.572680684675));
#67373=CARTESIAN_POINT('Ctrl Pts',(-24.4345859024878,19.7162122633372,-50.5785453716132));
#67374=CARTESIAN_POINT('Ctrl Pts',(-24.546656706582,19.7455623051099,-50.5844100585514));
#67375=CARTESIAN_POINT('Ctrl Pts',(-24.6586122528693,19.7748821622018,-50.5902687140261));
#67376=CARTESIAN_POINT('Ctrl Pts',(-24.769392701363,19.8091792226978,-50.5961273695009));
#67377=CARTESIAN_POINT('Ctrl Pts',(-24.8785253833609,19.8483367801508,-50.6019860249757));
#67378=CARTESIAN_POINT('Ctrl Pts',(-24.9919208840411,19.8890238662877,-50.6080735246936));
#67379=CARTESIAN_POINT('Ctrl Pts',(-25.1035368192879,19.9349588248107,-50.6141610244115));
#67380=CARTESIAN_POINT('Ctrl Pts',(-25.2128585695035,19.9859531386802,-50.6202485241294));
#67381=CARTESIAN_POINT('Ctrl Pts',(-25.3179487886732,20.0349736090842,-50.6261003942128));
#67382=CARTESIAN_POINT('Ctrl Pts',(-25.4209187134945,20.088668860267,-50.6319522642962));
#67383=CARTESIAN_POINT('Ctrl Pts',(-25.5213311898325,20.146822214583,-50.6378041343796));
#67384=CARTESIAN_POINT('Ctrl Pts',(-25.6217283774579,20.2049667145219,-50.6436551134626));
#67385=CARTESIAN_POINT('Ctrl Pts',(-25.7195685332179,20.2675677608329,-50.6495060925455));
#67386=CARTESIAN_POINT('Ctrl Pts',(-25.814439970529,20.3343631925187,-50.6553570716285));
#67387=CARTESIAN_POINT('Ctrl Pts',(-25.9093199376955,20.4011646297567,-50.6612085767708));
#67388=CARTESIAN_POINT('Ctrl Pts',(-26.0012303177777,20.4721609640463,-50.6670600819131));
#67389=CARTESIAN_POINT('Ctrl Pts',(-26.0897898217878,20.5470476848308,-50.6729115870554));
#67390=CARTESIAN_POINT('Ctrl Pts',(-26.1783787344812,20.621959273865,-50.6787650353551));
#67391=CARTESIAN_POINT('Ctrl Pts',(-26.2636142429747,20.7007635515012,-50.6846184836549));
#67392=CARTESIAN_POINT('Ctrl Pts',(-26.3451499924511,20.7831173373363,-50.6904719319547));
#67393=CARTESIAN_POINT('Ctrl Pts',(-26.42677846578,20.8655647773087,-50.6963320368962));
#67394=CARTESIAN_POINT('Ctrl Pts',(-26.5046984911743,20.9515694883994,-50.7021921418378));
#67395=CARTESIAN_POINT('Ctrl Pts',(-26.5786022228291,21.0407531497052,-50.7080522467793));
#67396=CARTESIAN_POINT('Ctrl Pts',(-26.6525557240218,21.1299968706252,-50.7139162981348));
#67397=CARTESIAN_POINT('Ctrl Pts',(-26.7224872970213,21.2224234757153,-50.7197803494902));
#67398=CARTESIAN_POINT('Ctrl Pts',(-26.7881318937342,21.3176248787088,-50.7256444008457));
#67399=CARTESIAN_POINT('Ctrl Pts',(-26.8538732374787,21.412966589566,-50.7315170946423));
#67400=CARTESIAN_POINT('Ctrl Pts',(-26.9153147765724,21.5110909111264,-50.7373897884388));
#67401=CARTESIAN_POINT('Ctrl Pts',(-26.9722368844682,21.6115642923505,-50.7432624822354));
#67402=CARTESIAN_POINT('Ctrl Pts',(-26.9878212054197,21.6390722234156,-50.7448703275588));
#67403=CARTESIAN_POINT('Ctrl Pts',(-27.0030670394137,21.6667561153043,-50.7464781728821));
#67404=CARTESIAN_POINT('Ctrl Pts',(-27.0179705123824,21.6946068202471,-50.7480860182055));
#67405=CARTESIAN_POINT('Ctrl Pts',(-27.0754310621943,21.8019856051811,-50.7542850884817));
#67406=CARTESIAN_POINT('Ctrl Pts',(-27.1279738091353,21.9121727179392,-50.7604841587579));
#67407=CARTESIAN_POINT('Ctrl Pts',(-27.1753306576848,22.0247042432207,-50.7666832290342));
#67408=CARTESIAN_POINT('Ctrl Pts',(-27.2225983833257,22.1370239905409,-50.772870633011));
#67409=CARTESIAN_POINT('Ctrl Pts',(-27.264699519378,22.2516790441243,-50.7790580369878));
#67410=CARTESIAN_POINT('Ctrl Pts',(-27.30141184107,22.368181114358,-50.7852454409647));
#67411=CARTESIAN_POINT('Ctrl Pts',(-27.3380337747153,22.4843963491621,-50.7914176111635));
#67412=CARTESIAN_POINT('Ctrl Pts',(-27.3692932407326,22.6024492064155,-50.7975897813623));
#67413=CARTESIAN_POINT('Ctrl Pts',(-27.3950164309745,22.7218326147495,-50.8037619515611));
#67414=CARTESIAN_POINT('Ctrl Pts',(-27.4207007736102,22.8410357281977,-50.8099248004418));
#67415=CARTESIAN_POINT('Ctrl Pts',(-27.4408654193857,22.9615650546885,-50.8160876493226));
#67416=CARTESIAN_POINT('Ctrl Pts',(-27.4553861962024,23.0828982096596,-50.8222504982033));
#67417=CARTESIAN_POINT('Ctrl Pts',(-27.4698793086307,23.2040002056798,-50.8284016058771));
#67418=CARTESIAN_POINT('Ctrl Pts',(-27.4787499437123,23.3259026354998,-50.8345527135509));
#67419=CARTESIAN_POINT('Ctrl Pts',(-27.4819250050777,23.4480734632001,-50.8407038212247));
#67420=CARTESIAN_POINT('Ctrl Pts',(-27.4828081251522,23.4820543845235,-50.8424147067925));
#67421=CARTESIAN_POINT('Ctrl Pts',(-27.4832509209801,23.5160560114756,-50.8441255923602));
#67422=CARTESIAN_POINT('Ctrl Pts',(-27.4832525273076,23.5500667762137,-50.845836477928));
#67423=CARTESIAN_POINT('',(-27.4832508703214,23.5538675497877,-52.095836477965));
#67424=CARTESIAN_POINT('Ctrl Pts',(-27.4832525273076,23.5500667769491,-50.845836477965));
#67425=CARTESIAN_POINT('Ctrl Pts',(-27.4832582621366,23.6714907668338,-50.8519446191219));
#67426=CARTESIAN_POINT('Ctrl Pts',(-27.4776365755207,23.7928145505648,-50.8580527602788));
#67427=CARTESIAN_POINT('Ctrl Pts',(-27.4664411021963,23.913510126616,-50.8641609014358));
#67428=CARTESIAN_POINT('Ctrl Pts',(-27.4552314451803,24.0343586134725,-50.8702767810767));
#67429=CARTESIAN_POINT('Ctrl Pts',(-27.4384339508407,24.154576949595,-50.8763926607176));
#67430=CARTESIAN_POINT('Ctrl Pts',(-27.4161536553574,24.273645579808,-50.8825085403585));
#67431=CARTESIAN_POINT('Ctrl Pts',(-27.3938220497938,24.3929884173797,-50.8886385044749));
#67432=CARTESIAN_POINT('Ctrl Pts',(-27.365982471607,24.5111759044408,-50.8947684685913));
#67433=CARTESIAN_POINT('Ctrl Pts',(-27.3327906542758,24.6277006052536,-50.9008984327076));
#67434=CARTESIAN_POINT('Ctrl Pts',(-27.2995573770958,24.7443708568941,-50.9070360537529));
#67435=CARTESIAN_POINT('Ctrl Pts',(-27.2609586372413,24.8593738402802,-50.9131736747982));
#67436=CARTESIAN_POINT('Ctrl Pts',(-27.2171987729359,24.9722209785464,-50.9193112958435));
#67437=CARTESIAN_POINT('Ctrl Pts',(-27.1733410876714,25.0853203757138,-50.9254626369491));
#67438=CARTESIAN_POINT('Ctrl Pts',(-27.1242993608469,25.1962539673951,-50.9316139780547));
#67439=CARTESIAN_POINT('Ctrl Pts',(-27.0703249722303,25.3045555310014,-50.9377653191603));
#67440=CARTESIAN_POINT('Ctrl Pts',(-27.0433945227279,25.3585924522985,-50.9408345226337));
#67441=CARTESIAN_POINT('Ctrl Pts',(-27.0152367819953,25.4119745593238,-50.9439037261071));
#67442=CARTESIAN_POINT('Ctrl Pts',(-26.9858869787784,25.464646677634,-50.9469729295805));
#67443=CARTESIAN_POINT('Ctrl Pts',(-26.9297320962635,25.5654240693478,-50.9528452265492));
#67444=CARTESIAN_POINT('Ctrl Pts',(-26.8690452280656,25.6638974107016,-50.9587175235178));
#67445=CARTESIAN_POINT('Ctrl Pts',(-26.804040216488,25.7596313363097,-50.9645898204865));
#67446=CARTESIAN_POINT('Ctrl Pts',(-26.7391194462429,25.855241198353,-50.9704545074247));
#67447=CARTESIAN_POINT('Ctrl Pts',(-26.6698918910716,25.9481183656194,-50.9763191943629));
#67448=CARTESIAN_POINT('Ctrl Pts',(-26.5966172610651,26.0378519640074,-50.9821838813011));
#67449=CARTESIAN_POINT('Ctrl Pts',(-26.5234179894285,26.1274932770068,-50.9880425367759));
#67450=CARTESIAN_POINT('Ctrl Pts',(-26.4461801816037,26.2139971333922,-50.9939011922507));
#67451=CARTESIAN_POINT('Ctrl Pts',(-26.3652064404348,26.2969821309933,-50.9997598477255));
#67452=CARTESIAN_POINT('Ctrl Pts',(-26.2810697936146,26.3832085956935,-51.0058473474434));
#67453=CARTESIAN_POINT('Ctrl Pts',(-26.1928996613371,26.4656353218793,-51.0119348471613));
#67454=CARTESIAN_POINT('Ctrl Pts',(-26.1010813966376,26.543872598064,-51.0180223468792));
#67455=CARTESIAN_POINT('Ctrl Pts',(-26.012817153319,26.6190815339368,-51.0238742169625));
#67456=CARTESIAN_POINT('Ctrl Pts',(-25.9211822877098,26.6904190193286,-51.0297260870459));
#67457=CARTESIAN_POINT('Ctrl Pts',(-25.8265555690924,26.7575775046166,-51.0355779571293));
#67458=CARTESIAN_POINT('Ctrl Pts',(-25.7319432582533,26.8247257644146,-51.0414289362123));
#67459=CARTESIAN_POINT('Ctrl Pts',(-25.6343403371765,26.8876960500704,-51.0472799152952));
#67460=CARTESIAN_POINT('Ctrl Pts',(-25.5341563588103,26.9462228797323,-51.0531308943781));
#67461=CARTESIAN_POINT('Ctrl Pts',(-25.4339633729406,27.0047549715193,-51.0589823995204));
#67462=CARTESIAN_POINT('Ctrl Pts',(-25.3311892254228,27.0588426045912,-51.0648339046627));
#67463=CARTESIAN_POINT('Ctrl Pts',(-25.2262693535155,27.1082655464219,-51.0706854098049));
#67464=CARTESIAN_POINT('Ctrl Pts',(-25.1213146400026,27.1577049005359,-51.0765388581047));
#67465=CARTESIAN_POINT('Ctrl Pts',(-25.0142131590139,27.2024763071687,-51.0823923064045));
#67466=CARTESIAN_POINT('Ctrl Pts',(-24.9054209997638,27.2424073799027,-51.0882457547042));
#67467=CARTESIAN_POINT('Ctrl Pts',(-24.7965051202049,27.2823838629373,-51.0941058596457));
#67468=CARTESIAN_POINT('Ctrl Pts',(-24.6858951130954,27.3175088827148,-51.0999659645872));
#67469=CARTESIAN_POINT('Ctrl Pts',(-24.5740630237384,27.3476596834729,-51.1058260695288));
#67470=CARTESIAN_POINT('Ctrl Pts',(-24.4621556224685,27.3778307889083,-51.1116901208842));
#67471=CARTESIAN_POINT('Ctrl Pts',(-24.3490249027182,27.4030209155317,-51.1175541722396));
#67472=CARTESIAN_POINT('Ctrl Pts',(-24.2351521945031,27.4231586049013,-51.123418223595));
#67473=CARTESIAN_POINT('Ctrl Pts',(-24.1211116606473,27.4433259732051,-51.1292909173916));
#67474=CARTESIAN_POINT('Ctrl Pts',(-24.006327364139,27.4584259891948,-51.1351636111881));
#67475=CARTESIAN_POINT('Ctrl Pts',(-23.8912849176308,27.4684390907726,-51.1410363049847));
#67476=CARTESIAN_POINT('Ctrl Pts',(-23.8597882201984,27.4711805104861,-51.1426441503082));
#67477=CARTESIAN_POINT('Ctrl Pts',(-23.8282721648829,27.4735409303254,-51.1442519956317));
#67478=CARTESIAN_POINT('Ctrl Pts',(-23.7967466820691,27.4755206287585,-51.1458598409552));
#67479=CARTESIAN_POINT('Ctrl Pts',(-23.6816068769783,27.4827510363965,-51.1517321379239));
#67480=CARTESIAN_POINT('Ctrl Pts',(-23.565955777727,27.4849231715453,-51.1576044348926));
#67481=CARTESIAN_POINT('Ctrl Pts',(-23.4502752553495,27.4819816098753,-51.1634767318613));
#67482=CARTESIAN_POINT('Ctrl Pts',(-23.3347446457418,27.4790438602355,-51.1693414187995));
#67483=CARTESIAN_POINT('Ctrl Pts',(-23.2191850982695,27.4710056028029,-51.1752061057377));
#67484=CARTESIAN_POINT('Ctrl Pts',(-23.1040826725221,27.4578632411644,-51.1810707926759));
#67485=CARTESIAN_POINT('Ctrl Pts',(-22.9890986224141,27.4447343956222,-51.1869294481508));
#67486=CARTESIAN_POINT('Ctrl Pts',(-22.8745711671811,27.426511933519,-51.1927881036256));
#67487=CARTESIAN_POINT('Ctrl Pts',(-22.7609847565337,27.4032442756632,-51.1986467591004));
#67488=CARTESIAN_POINT('Ctrl Pts',(-22.6429615606407,27.3790677625976,-51.2047342588183));
#67489=CARTESIAN_POINT('Ctrl Pts',(-22.5259548786314,27.3494438907925,-51.2108217585362));
#67490=CARTESIAN_POINT('Ctrl Pts',(-22.4105008809704,27.3144862086426,-51.2169092582541));
#67491=CARTESIAN_POINT('Ctrl Pts',(-22.2995157760456,27.2808816379916,-51.2227611283376));
#67492=CARTESIAN_POINT('Ctrl Pts',(-22.1899658231277,27.2423486231468,-51.228612998421));
#67493=CARTESIAN_POINT('Ctrl Pts',(-22.0823145097288,27.1990395854517,-51.2344648685044));
#67494=CARTESIAN_POINT('Ctrl Pts',(-21.9746795872214,27.1557371419514,-51.2403158475873));
#67495=CARTESIAN_POINT('Ctrl Pts',(-21.8689431128443,27.1076602757401,-51.2461668266703));
#67496=CARTESIAN_POINT('Ctrl Pts',(-21.7655498216647,27.0550100463895,-51.2520178057533));
#67497=CARTESIAN_POINT('Ctrl Pts',(-21.6621472344333,27.0023550832766,-51.2578693108956));
#67498=CARTESIAN_POINT('Ctrl Pts',(-21.5610886175952,26.9451261272124,-51.2637208160379));
#67499=CARTESIAN_POINT('Ctrl Pts',(-21.4627946287674,26.8835704738516,-51.2695723211802));
#67500=CARTESIAN_POINT('Ctrl Pts',(-21.364467998646,26.8219943791985,-51.2754257694799));
#67501=CARTESIAN_POINT('Ctrl Pts',(-21.2689081722319,26.7560889495473,-51.2812792177797));
#67502=CARTESIAN_POINT('Ctrl Pts',(-21.1765067166659,26.6861447182394,-51.2871326660794));
#67503=CARTESIAN_POINT('Ctrl Pts',(-21.0840001805799,26.6161209451522,-51.292992771021));
#67504=CARTESIAN_POINT('Ctrl Pts',(-20.994659514171,26.5420494525735,-51.2988528759625));
#67505=CARTESIAN_POINT('Ctrl Pts',(-20.9088431544191,26.4642610254436,-51.3047129809041));
#67506=CARTESIAN_POINT('Ctrl Pts',(-20.8229690027202,26.3864202126767,-51.3105770322595));
#67507=CARTESIAN_POINT('Ctrl Pts',(-20.7406241765691,26.3048577713405,-51.3164410836149));
#67508=CARTESIAN_POINT('Ctrl Pts',(-20.6621289744305,26.2199400261359,-51.3223051349704));
#67509=CARTESIAN_POINT('Ctrl Pts',(-20.5835180860329,26.134897129126,-51.3281778287669));
#67510=CARTESIAN_POINT('Ctrl Pts',(-20.5087684109145,26.0464893733715,-51.3340505225635));
#67511=CARTESIAN_POINT('Ctrl Pts',(-20.4381589012217,25.9551147388014,-51.3399232163601));
#67512=CARTESIAN_POINT('Ctrl Pts',(-20.4188271986202,25.9300978923664,-51.3415310616835));
#67513=CARTESIAN_POINT('Ctrl Pts',(-20.3998055738489,25.9048588132359,-51.3431389070068));
#67514=CARTESIAN_POINT('Ctrl Pts',(-20.3810991604219,25.8794060065329,-51.3447467523302));
#67515=CARTESIAN_POINT('Ctrl Pts',(-20.312778151388,25.7864452985128,-51.3506190492989));
#67516=CARTESIAN_POINT('Ctrl Pts',(-20.2484363756992,25.6903202194212,-51.3564913462677));
#67517=CARTESIAN_POINT('Ctrl Pts',(-20.188380934496,25.5914062162441,-51.3623636432364));
#67518=CARTESIAN_POINT('Ctrl Pts',(-20.1284033203751,25.4926203977597,-51.3682283301746));
#67519=CARTESIAN_POINT('Ctrl Pts',(-20.0727012068954,25.3910531926764,-51.3740930171128));
#67520=CARTESIAN_POINT('Ctrl Pts',(-20.021540355593,25.2871115870683,-51.379957704051));
#67521=CARTESIAN_POINT('Ctrl Pts',(-19.9704321200234,25.1832768788948,-51.3858163595258));
#67522=CARTESIAN_POINT('Ctrl Pts',(-19.9238560384149,25.0770729959655,-51.3916750150006));
#67523=CARTESIAN_POINT('Ctrl Pts',(-19.882033239135,24.9689336874498,-51.3975336704755));
#67524=CARTESIAN_POINT('Ctrl Pts',(-19.8385768044781,24.8565703622957,-51.4036211701934));
#67525=CARTESIAN_POINT('Ctrl Pts',(-19.800252792973,24.7421177189986,-51.4097086699113));
#67526=CARTESIAN_POINT('Ctrl Pts',(-19.7672554973163,24.6260882244875,-51.4157961696292));
#67527=CARTESIAN_POINT('Ctrl Pts',(-19.7355354322263,24.5145498985429,-51.4216480397126));
#67528=CARTESIAN_POINT('Ctrl Pts',(-19.7087375104274,24.4015549570428,-51.427499909796));
#67529=CARTESIAN_POINT('Ctrl Pts',(-19.6869840319349,24.2875757300053,-51.4333517798794));
#67530=CARTESIAN_POINT('Ctrl Pts',(-19.6652338656073,24.1736138573415,-51.4392027589624));
#67531=CARTESIAN_POINT('Ctrl Pts',(-19.6485266929083,24.058668403065,-51.4450537380454));
#67532=CARTESIAN_POINT('Ctrl Pts',(-19.6369337572042,23.9432222114717,-51.4509047171283));
#67533=CARTESIAN_POINT('Ctrl Pts',(-19.6253397791837,23.8277656401547,-51.4567562222706));
#67534=CARTESIAN_POINT('Ctrl Pts',(-19.6188609935423,23.7118086533619,-51.462607727413));
#67535=CARTESIAN_POINT('Ctrl Pts',(-19.6175167295714,23.5958388311891,-51.4684592325553));
#67536=CARTESIAN_POINT('Ctrl Pts',(-19.6161720191997,23.4798304979626,-51.4743126808551));
#67537=CARTESIAN_POINT('Ctrl Pts',(-19.6199652256975,23.3638097340171,-51.4801661291549));
#67538=CARTESIAN_POINT('Ctrl Pts',(-19.6288635771295,23.2482630169458,-51.4860195774547));
#67539=CARTESIAN_POINT('Ctrl Pts',(-19.6377720479193,23.132584898167,-51.4918796823962));
#67540=CARTESIAN_POINT('Ctrl Pts',(-19.6517972198019,23.017382314685,-51.4977397873378));
#67541=CARTESIAN_POINT('Ctrl Pts',(-19.6708545482404,22.9031356288285,-51.5035998922793));
#67542=CARTESIAN_POINT('Ctrl Pts',(-19.6899247105968,22.7888120049794,-51.5094639436348));
#67543=CARTESIAN_POINT('Ctrl Pts',(-19.7140336915884,22.6754459639168,-51.5153279949902));
#67544=CARTESIAN_POINT('Ctrl Pts',(-19.7430464309964,22.5635049921435,-51.5211920463457));
#67545=CARTESIAN_POINT('Ctrl Pts',(-19.7721019293908,22.4513990417234,-51.5270647401423));
#67546=CARTESIAN_POINT('Ctrl Pts',(-19.8060754893694,22.3407227460215,-51.5329374339388));
#67547=CARTESIAN_POINT('Ctrl Pts',(-19.8447830692011,22.2319259171821,-51.5388101277354));
#67548=CARTESIAN_POINT('Ctrl Pts',(-19.8553805570597,22.2021391653961,-51.5404179730587));
#67549=CARTESIAN_POINT('Ctrl Pts',(-19.8663326232262,22.1724931610982,-51.5420258183819));
#67550=CARTESIAN_POINT('Ctrl Pts',(-19.8776348870796,22.1429968205794,-51.5436336637052));
#67551=CARTESIAN_POINT('Ctrl Pts',(-19.9189138887385,22.0352680058037,-51.5495059606738));
#67552=CARTESIAN_POINT('Ctrl Pts',(-19.9650060731872,21.9291765100944,-51.5553782576425));
#67553=CARTESIAN_POINT('Ctrl Pts',(-20.0157615717623,21.8251836478059,-51.5612505546112));
#67554=CARTESIAN_POINT('Ctrl Pts',(-20.0664512952421,21.721325552008,-51.5671152415494));
#67555=CARTESIAN_POINT('Ctrl Pts',(-20.1217921352823,21.6195610492669,-51.5729799284876));
#67556=CARTESIAN_POINT('Ctrl Pts',(-20.1815853430468,21.5203337224483,-51.5788446154258));
#67557=CARTESIAN_POINT('Ctrl Pts',(-20.2413170572404,21.4212084447233,-51.5847032709007));
#67558=CARTESIAN_POINT('Ctrl Pts',(-20.3054918192543,21.3246155047753,-51.5905619263755));
#67559=CARTESIAN_POINT('Ctrl Pts',(-20.3738642378916,21.2309754014241,-51.5964205818503));
#67560=CARTESIAN_POINT('Ctrl Pts',(-20.4449073434223,21.1336776331592,-51.6025080815682));
#67561=CARTESIAN_POINT('Ctrl Pts',(-20.5204825196542,21.0395684935762,-51.6085955812861));
#67562=CARTESIAN_POINT('Ctrl Pts',(-20.6002636430009,20.9490884544807,-51.614683081004));
#67563=CARTESIAN_POINT('Ctrl Pts',(-20.6769566681454,20.8621106378952,-51.6205349510874));
#67564=CARTESIAN_POINT('Ctrl Pts',(-20.7575357955095,20.7784865405874,-51.6263868211708));
#67565=CARTESIAN_POINT('Ctrl Pts',(-20.841669754267,20.6985743700103,-51.6322386912542));
#67566=CARTESIAN_POINT('Ctrl Pts',(-20.9257909028643,20.6186743667879,-51.6380896703372));
#67567=CARTESIAN_POINT('Ctrl Pts',(-21.013465507019,20.542485451159,-51.6439406494201));
#67568=CARTESIAN_POINT('Ctrl Pts',(-21.1043258517836,20.4703285591745,-51.6497916285031));
#67569=CARTESIAN_POINT('Ctrl Pts',(-21.1951943657672,20.3981651795913,-51.6556431336454));
#67570=CARTESIAN_POINT('Ctrl Pts',(-21.289248866016,20.3300348014017,-51.6614946387876));
#67571=CARTESIAN_POINT('Ctrl Pts',(-21.386089591516,20.2662172443748,-51.6673461439299));
#67572=CARTESIAN_POINT('Ctrl Pts',(-21.4829624757136,20.2023784949259,-51.6731995922297));
#67573=CARTESIAN_POINT('Ctrl Pts',(-21.5826230799634,20.1428556418139,-51.6790530405295));
#67574=CARTESIAN_POINT('Ctrl Pts',(-21.6846444078837,20.0878840752222,-51.6849064888293));
#67575=CARTESIAN_POINT('Ctrl Pts',(-21.7867817562068,20.0328499940227,-51.6907665937708));
#67576=CARTESIAN_POINT('Ctrl Pts',(-21.891284822559,19.9823777262893,-51.6966266987124));
#67577=CARTESIAN_POINT('Ctrl Pts',(-21.9977037701475,19.9366557994868,-51.7024868036539));
#67578=CARTESIAN_POINT('Ctrl Pts',(-22.104194384237,19.8909030818281,-51.7083508550093));
#67579=CARTESIAN_POINT('Ctrl Pts',(-22.2126030629448,19.8499072209206,-51.7142149063648));
#67580=CARTESIAN_POINT('Ctrl Pts',(-22.3224634962584,19.8138072846093,-51.7200789577203));
#67581=CARTESIAN_POINT('Ctrl Pts',(-22.4324858419203,19.7776541441981,-51.7259516515168));
#67582=CARTESIAN_POINT('Ctrl Pts',(-22.5439638158583,19.7464114404966,-51.7318243453134));
#67583=CARTESIAN_POINT('Ctrl Pts',(-22.6564195012106,19.7201674786416,-51.73769703911));
#67584=CARTESIAN_POINT('Ctrl Pts',(-22.6872079867061,19.7129823208937,-51.7393048844333));
#67585=CARTESIAN_POINT('Ctrl Pts',(-22.7180697235853,19.7061715558093,-51.7409127297566));
#67586=CARTESIAN_POINT('Ctrl Pts',(-22.7489948425118,19.699736317532,-51.74252057508));
#67587=CARTESIAN_POINT('Ctrl Pts',(-22.8619419522212,19.676233042882,-51.7483928720487));
#67588=CARTESIAN_POINT('Ctrl Pts',(-22.9761132872718,19.6576642200362,-51.7542651690174));
#67589=CARTESIAN_POINT('Ctrl Pts',(-23.0910397257914,19.6441531219384,-51.7601374659861));
#67590=CARTESIAN_POINT('Ctrl Pts',(-23.2058172287738,19.6306595331507,-51.7660021529243));
#67591=CARTESIAN_POINT('Ctrl Pts',(-23.3213474824664,19.6222106825637,-51.7718668398625));
#67592=CARTESIAN_POINT('Ctrl Pts',(-23.4371498609902,19.6188791347908,-51.7777315268007));
#67593=CARTESIAN_POINT('Ctrl Pts',(-23.5528331440167,19.6155510133062,-51.7835901822755));
#67594=CARTESIAN_POINT('Ctrl Pts',(-23.6687875844842,19.6173297384213,-51.7894488377503));
#67595=CARTESIAN_POINT('Ctrl Pts',(-23.7845267653356,19.624236155843,-51.7953074932251));
#67596=CARTESIAN_POINT('Ctrl Pts',(-23.9047868205333,19.6314123440124,-51.801394992943));
#67597=CARTESIAN_POINT('Ctrl Pts',(-24.0248140052634,19.644125028281,-51.8074824926609));
#67598=CARTESIAN_POINT('Ctrl Pts',(-24.1440614595818,19.6623379290877,-51.8135699923788));
#67599=CARTESIAN_POINT('Ctrl Pts',(-24.2586931873493,19.6798458608005,-51.8194218624622));
#67600=CARTESIAN_POINT('Ctrl Pts',(-24.3726039778124,19.7024360629564,-51.8252737325456));
#67601=CARTESIAN_POINT('Ctrl Pts',(-24.4853133991054,19.7300234581652,-51.831125602629));
#67602=CARTESIAN_POINT('Ctrl Pts',(-24.598005659364,19.7576066529422,-51.836976581712));
#67603=CARTESIAN_POINT('Ctrl Pts',(-24.7094965127351,19.790185429669,-51.842827560795));
#67604=CARTESIAN_POINT('Ctrl Pts',(-24.8193171848167,19.8276239031314,-51.848678539878));
#67605=CARTESIAN_POINT('Ctrl Pts',(-24.929147730833,19.8650657426727,-51.8545300450202));
#67606=CARTESIAN_POINT('Ctrl Pts',(-25.0373074057501,19.9073680141385,-51.8603815501625));
#67607=CARTESIAN_POINT('Ctrl Pts',(-25.1433447047262,19.954345646328,-51.8662330553048));
#67608=CARTESIAN_POINT('Ctrl Pts',(-25.2494172163824,20.0013388787671,-51.8720865036046));
#67609=CARTESIAN_POINT('Ctrl Pts',(-25.3533655729051,20.0530103917931,-51.8779399519045));
#67610=CARTESIAN_POINT('Ctrl Pts',(-25.4547609269378,20.109128184559,-51.8837934002043));
#67611=CARTESIAN_POINT('Ctrl Pts',(-25.5562715895045,20.1653097954403,-51.8896535051458));
#67612=CARTESIAN_POINT('Ctrl Pts',(-25.6552230927477,20.2259475781596,-51.8955136100874));
#67613=CARTESIAN_POINT('Ctrl Pts',(-25.7512136694914,20.2907649845625,-51.9013737150289));
#67614=CARTESIAN_POINT('Ctrl Pts',(-25.8472688898812,20.3556260414322,-51.9072377663844));
#67615=CARTESIAN_POINT('Ctrl Pts',(-25.940358882113,20.4246720809784,-51.9131018177399));
#67616=CARTESIAN_POINT('Ctrl Pts',(-26.0301145857459,20.4975859608296,-51.9189658690953));
#67617=CARTESIAN_POINT('Ctrl Pts',(-26.1200025713687,20.5706073011844,-51.9248385628919));
#67618=CARTESIAN_POINT('Ctrl Pts',(-26.2065461529907,20.6475075852407,-51.9307112566885));
#67619=CARTESIAN_POINT('Ctrl Pts',(-26.2894127036948,20.7279324661939,-51.9365839504851));
#67620=CARTESIAN_POINT('Ctrl Pts',(-26.3121001790887,20.7499514532541,-51.9381917958083));
#67621=CARTESIAN_POINT('Ctrl Pts',(-26.3345122671313,20.7722344430389,-51.9397996411316));
#67622=CARTESIAN_POINT('Ctrl Pts',(-26.356642678854,20.7947737453624,-51.9414074864549));
#67623=CARTESIAN_POINT('Ctrl Pts',(-26.4363906743046,20.8759951976191,-51.9472014338578));
#67624=CARTESIAN_POINT('Ctrl Pts',(-26.5127608102905,20.9608357359645,-51.9529953812607));
#67625=CARTESIAN_POINT('Ctrl Pts',(-26.5853998345252,21.0489788861053,-51.9587893286636));
#67626=CARTESIAN_POINT('Ctrl Pts',(-26.6579229415245,21.136981377552,-51.9645740300948));
#67627=CARTESIAN_POINT('Ctrl Pts',(-26.7267265150926,21.2282756699981,-51.9703587315259));
#67628=CARTESIAN_POINT('Ctrl Pts',(-26.7914935773824,21.3225080481983,-51.9761434329571));
#67629=CARTESIAN_POINT('Ctrl Pts',(-26.8562015787308,21.4166544961007,-51.9819228593317));
#67630=CARTESIAN_POINT('Ctrl Pts',(-26.9168801420518,21.5137333589691,-51.9877022857064));
#67631=CARTESIAN_POINT('Ctrl Pts',(-26.973252252748,21.6133576172331,-51.9934817120811));
#67632=CARTESIAN_POINT('Ctrl Pts',(-27.0295874781854,21.7129166896009,-51.9992573568759));
#67633=CARTESIAN_POINT('Ctrl Pts',(-27.0816216417915,21.8150174787474,-52.0050330016708));
#67634=CARTESIAN_POINT('Ctrl Pts',(-27.1291213003051,21.9192444578142,-52.0108086464656));
#67635=CARTESIAN_POINT('Ctrl Pts',(-27.1766021097159,22.0234300768986,-52.016581999334));
#67636=CARTESIAN_POINT('Ctrl Pts',(-27.2195518154751,22.1297398218363,-52.0223553522024));
#67637=CARTESIAN_POINT('Ctrl Pts',(-27.2577835617444,22.2377348513505,-52.0281287050708));
#67638=CARTESIAN_POINT('Ctrl Pts',(-27.2960234093541,22.3457527651056,-52.0339032813177));
#67639=CARTESIAN_POINT('Ctrl Pts',(-27.3295431476156,22.4554562793153,-52.0396778575646));
#67640=CARTESIAN_POINT('Ctrl Pts',(-27.3582047519617,22.5663882686172,-52.0454524338115));
#67641=CARTESIAN_POINT('Ctrl Pts',(-27.3868682813938,22.6773277087797,-52.0512273979138));
#67642=CARTESIAN_POINT('Ctrl Pts',(-27.4106729294253,22.7894953738474,-52.057002362016));
#67643=CARTESIAN_POINT('Ctrl Pts',(-27.4295314336681,22.9024221521192,-52.0627773261183));
#67644=CARTESIAN_POINT('Ctrl Pts',(-27.4484075946599,23.0154546609279,-52.0685576971759));
#67645=CARTESIAN_POINT('Ctrl Pts',(-27.4623282990379,23.1292472810354,-52.0743380682336));
#67646=CARTESIAN_POINT('Ctrl Pts',(-27.4712579968975,23.2433239702244,-52.0801184392912));
#67647=CARTESIAN_POINT('Ctrl Pts',(-27.4793519026867,23.3467234345241,-52.0853577855158));
#67648=CARTESIAN_POINT('Ctrl Pts',(-27.4833460130466,23.4503559848456,-52.0905971317404));
#67649=CARTESIAN_POINT('Ctrl Pts',(-27.4832508703214,23.5538675497877,-52.095836477965));
#67650=CARTESIAN_POINT('',(-27.4847156486848,23.548792864961,-53.345836477965));
#67651=CARTESIAN_POINT('Ctrl Pts',(-27.4836164097124,23.5538678857735,-52.095836477965));
#67652=CARTESIAN_POINT('Ctrl Pts',(-27.4863365027118,23.8466766674494,-52.1106557845866));
#67653=CARTESIAN_POINT('Ctrl Pts',(-27.3226060095439,25.4463805907666,-52.1917707283331));
#67654=CARTESIAN_POINT('Ctrl Pts',(-25.1349592851244,27.9239758125807,-52.3391813092048));
#67655=CARTESIAN_POINT('Ctrl Pts',(-20.7271669327941,27.2476757605631,-52.5380682205796));
#67656=CARTESIAN_POINT('Ctrl Pts',(-18.9135508876664,23.1737572510144,-52.7369551319543));
#67657=CARTESIAN_POINT('Ctrl Pts',(-21.3606705259297,19.4458059828712,-52.9358420433294));
#67658=CARTESIAN_POINT('Ctrl Pts',(-25.8198303815515,19.4894930934187,-53.1347289547041));
#67659=CARTESIAN_POINT('Ctrl Pts',(-27.4508527243426,22.083602281584,-53.2713937662495));
#67660=CARTESIAN_POINT('Ctrl Pts',(-27.4894817226864,23.4685949761432,-53.3417629406697));
#67661=CARTESIAN_POINT('Ctrl Pts',(-27.4891003288786,23.5487912382659,-53.345836477965));
#67662=CARTESIAN_POINT('',(-27.4826585752767,23.5473454798973,-54.5958364365128));
#67663=CARTESIAN_POINT('Ctrl Pts',(-27.4832522610303,23.5487934078707,-53.345836477965));
#67664=CARTESIAN_POINT('Ctrl Pts',(-27.4832946914238,23.663162540572,-53.3516544617535));
#67665=CARTESIAN_POINT('Ctrl Pts',(-27.4783442215885,23.7777353956967,-53.3574724455419));
#67666=CARTESIAN_POINT('Ctrl Pts',(-27.4683737448524,23.8920348586218,-53.3632904293304));
#67667=CARTESIAN_POINT('Ctrl Pts',(-27.4584157308707,24.006191451132,-53.3691011408383));
#67668=CARTESIAN_POINT('Ctrl Pts',(-27.4434502201329,24.1200749146401,-53.3749118523463));
#67669=CARTESIAN_POINT('Ctrl Pts',(-27.4235021021631,24.2332069700445,-53.3807225638542));
#67670=CARTESIAN_POINT('Ctrl Pts',(-27.4035733411655,24.3462292459676,-53.3865276368462));
#67671=CARTESIAN_POINT('Ctrl Pts',(-27.3786716594561,24.4585011507698,-53.3923327098383));
#67672=CARTESIAN_POINT('Ctrl Pts',(-27.3488737818166,24.5695491509951,-53.3981377828303));
#67673=CARTESIAN_POINT('Ctrl Pts',(-27.3190951784397,24.6805253216648,-53.4039391009072));
#67674=CARTESIAN_POINT('Ctrl Pts',(-27.2844267847394,24.7902787557818,-53.4097404189842));
#67675=CARTESIAN_POINT('Ctrl Pts',(-27.2449963344048,24.8983464573282,-53.4155417370611));
#67676=CARTESIAN_POINT('Ctrl Pts',(-27.2055788649269,25.0063785820212,-53.4213411452922));
#67677=CARTESIAN_POINT('Ctrl Pts',(-27.1614025985756,25.1127256813328,-53.4271405535234));
#67678=CARTESIAN_POINT('Ctrl Pts',(-27.1126447980758,25.2169409670127,-53.4329399617545));
#67679=CARTESIAN_POINT('Ctrl Pts',(-27.063890716047,25.3211483048052,-53.4387389276989));
#67680=CARTESIAN_POINT('Ctrl Pts',(-27.0105559733405,25.4232237703927,-53.4445378936432));
#67681=CARTESIAN_POINT('Ctrl Pts',(-26.9528652022628,25.52274233245,-53.4503368595876));
#67682=CARTESIAN_POINT('Ctrl Pts',(-26.8951642377128,25.6222784785972,-53.4561368501603));
#67683=CARTESIAN_POINT('Ctrl Pts',(-26.833105927028,25.7192564588746,-53.461936840733));
#67684=CARTESIAN_POINT('Ctrl Pts',(-26.7669594764301,25.8132782566226,-53.4677368313057));
#67685=CARTESIAN_POINT('Ctrl Pts',(-26.70074402803,25.9073981291327,-53.4735428718871));
#67686=CARTESIAN_POINT('Ctrl Pts',(-26.6304321681201,25.9985553167895,-53.4793489124685));
#67687=CARTESIAN_POINT('Ctrl Pts',(-26.5563348674562,26.086383046991,-53.4851549530499));
#67688=CARTESIAN_POINT('Ctrl Pts',(-26.4821965350304,26.1742594122506,-53.4909642087561));
#67689=CARTESIAN_POINT('Ctrl Pts',(-26.404268874238,26.2588023399374,-53.4967734644624));
#67690=CARTESIAN_POINT('Ctrl Pts',(-26.3229000474504,26.339681640557,-53.5025827201687));
#67691=CARTESIAN_POINT('Ctrl Pts',(-26.241401802324,26.4206895809166,-53.5084012155832));
#67692=CARTESIAN_POINT('Ctrl Pts',(-26.1564517727988,26.4980219742657,-53.5142197109978));
#67693=CARTESIAN_POINT('Ctrl Pts',(-26.0684317427574,26.5713884870873,-53.5200382064123));
#67694=CARTESIAN_POINT('Ctrl Pts',(-26.0055786143933,26.6237778676163,-53.5241930634262));
#67695=CARTESIAN_POINT('Ctrl Pts',(-25.9411607548155,26.6741458817202,-53.52834792044));
#67696=CARTESIAN_POINT('Ctrl Pts',(-25.8753256237094,26.7224007181424,-53.5325027774539));
#67697=CARTESIAN_POINT('Ctrl Pts',(-25.7822770688398,26.7906020373943,-53.5383750744226));
#67698=CARTESIAN_POINT('Ctrl Pts',(-25.686069266483,26.8548200542966,-53.5442473713914));
#67699=CARTESIAN_POINT('Ctrl Pts',(-25.5870780585296,26.9147481511343,-53.5501196683601));
#67700=CARTESIAN_POINT('Ctrl Pts',(-25.4882151353203,26.9745985859177,-53.5559843552983));
#67701=CARTESIAN_POINT('Ctrl Pts',(-25.3865763300523,27.030169944172,-53.5618490422365));
#67702=CARTESIAN_POINT('Ctrl Pts',(-25.2825689704772,27.0811969883406,-53.5677137291747));
#67703=CARTESIAN_POINT('Ctrl Pts',(-25.1786685759603,27.1321715543888,-53.5735723846495));
#67704=CARTESIAN_POINT('Ctrl Pts',(-25.0724048411793,27.1786109212852,-53.5794310401243));
#67705=CARTESIAN_POINT('Ctrl Pts',(-24.9642117995196,27.2202945190468,-53.5852896955992));
#67706=CARTESIAN_POINT('Ctrl Pts',(-24.8517926423577,27.2636063148512,-53.5913771953171));
#67707=CARTESIAN_POINT('Ctrl Pts',(-24.7372907738129,27.3017830029639,-53.597464695035));
#67708=CARTESIAN_POINT('Ctrl Pts',(-24.6212189104289,27.3346309503542,-53.6035521947529));
#67709=CARTESIAN_POINT('Ctrl Pts',(-24.5096398555892,27.3662074480203,-53.6094040648363));
#67710=CARTESIAN_POINT('Ctrl Pts',(-24.3966105208159,27.3928599319203,-53.6152559349197));
#67711=CARTESIAN_POINT('Ctrl Pts',(-24.2826033931268,27.4144667099921,-53.6211078050031));
#67712=CARTESIAN_POINT('Ctrl Pts',(-24.1686136240595,27.4360701982356,-53.6269587840861));
#67713=CARTESIAN_POINT('Ctrl Pts',(-24.0536467641348,27.4526294312334,-53.6328097631691));
#67714=CARTESIAN_POINT('Ctrl Pts',(-23.9381857489335,27.4640737870612,-53.638660742252));
#67715=CARTESIAN_POINT('Ctrl Pts',(-23.8227143526758,27.4755191718467,-53.6445122473944));
#67716=CARTESIAN_POINT('Ctrl Pts',(-23.7067491242115,27.4818487244931,-53.6503637525366));
#67717=CARTESIAN_POINT('Ctrl Pts',(-23.5907776681084,27.4830437432027,-53.6562152576789));
#67718=CARTESIAN_POINT('Ctrl Pts',(-23.4747677004092,27.484239158752,-53.6620687059787));
#67719=CARTESIAN_POINT('Ctrl Pts',(-23.3587519141009,27.480296645689,-53.6679221542785));
#67720=CARTESIAN_POINT('Ctrl Pts',(-23.243216744199,27.4712496019809,-53.6737756025783));
#67721=CARTESIAN_POINT('Ctrl Pts',(-23.1275501857212,27.4621922698196,-53.6796357075199));
#67722=CARTESIAN_POINT('Ctrl Pts',(-23.0123657469431,27.4480188527795,-53.6854958124614));
#67723=CARTESIAN_POINT('Ctrl Pts',(-22.8981436809932,27.4288145135165,-53.691355917403));
#67724=CARTESIAN_POINT('Ctrl Pts',(-22.7838446936306,27.409597241333,-53.6972199687584));
#67725=CARTESIAN_POINT('Ctrl Pts',(-22.6705097728295,27.3853423870215,-53.7030840201139));
#67726=CARTESIAN_POINT('Ctrl Pts',(-22.5586062308937,27.3561856123078,-53.7089480714693));
#67727=CARTESIAN_POINT('Ctrl Pts',(-22.4465377654753,27.3269858663284,-53.7148207652659));
#67728=CARTESIAN_POINT('Ctrl Pts',(-22.3359052827544,27.292869902692,-53.7206934590625));
#67729=CARTESIAN_POINT('Ctrl Pts',(-22.2271583576552,27.2540223418503,-53.726566152859));
#67730=CARTESIAN_POINT('Ctrl Pts',(-22.1973852686777,27.2433865295325,-53.7281739981823));
#67731=CARTESIAN_POINT('Ctrl Pts',(-22.1677533833864,27.2323963203315,-53.7297818435056));
#67732=CARTESIAN_POINT('Ctrl Pts',(-22.1382716124275,27.2210561063393,-53.7313896888289));
#67733=CARTESIAN_POINT('Ctrl Pts',(-22.0305960097272,27.1796385002506,-53.7372619857976));
#67734=CARTESIAN_POINT('Ctrl Pts',(-21.9245639189295,27.1334098224602,-53.7431342827663));
#67735=CARTESIAN_POINT('Ctrl Pts',(-21.8206364611377,27.0825205351833,-53.749006579735));
#67736=CARTESIAN_POINT('Ctrl Pts',(-21.7168436850777,27.0316971963812,-53.7548712666732));
#67737=CARTESIAN_POINT('Ctrl Pts',(-21.6151504859665,26.9762254391619,-53.7607359536114));
#67738=CARTESIAN_POINT('Ctrl Pts',(-21.516000190528,26.9163045830534,-53.7666006405496));
#67739=CARTESIAN_POINT('Ctrl Pts',(-21.4169518649613,26.8564453517943,-53.7724592960244));
#67740=CARTESIAN_POINT('Ctrl Pts',(-21.3204415929319,26.7921463353161,-53.7783179514993));
#67741=CARTESIAN_POINT('Ctrl Pts',(-21.226889557112,26.7236534657617,-53.7841766069741));
#67742=CARTESIAN_POINT('Ctrl Pts',(-21.1296832963733,26.6524852043947,-53.790264106692));
#67743=CARTESIAN_POINT('Ctrl Pts',(-21.0356714940989,26.5767889795969,-53.7963516064099));
#67744=CARTESIAN_POINT('Ctrl Pts',(-20.9452942020338,26.4968914815374,-53.8024391061278));
#67745=CARTESIAN_POINT('Ctrl Pts',(-20.8584151554361,26.4200865862109,-53.8082909762112));
#67746=CARTESIAN_POINT('Ctrl Pts',(-20.7748948264504,26.3393999078589,-53.8141428462946));
#67747=CARTESIAN_POINT('Ctrl Pts',(-20.6950909959134,26.2551631780184,-53.819994716378));
#67748=CARTESIAN_POINT('Ctrl Pts',(-20.6152993162354,26.1709392739861,-53.825845695461));
#67749=CARTESIAN_POINT('Ctrl Pts',(-20.5392232940991,26.0831666932203,-53.8316966745439));
#67750=CARTESIAN_POINT('Ctrl Pts',(-20.4671833920689,25.9922135633837,-53.8375476536269));
#67751=CARTESIAN_POINT('Ctrl Pts',(-20.3951370129583,25.9012522559856,-53.8433991587692));
#67752=CARTESIAN_POINT('Ctrl Pts',(-20.3271277320184,25.80711015512,-53.8492506639115));
#67753=CARTESIAN_POINT('Ctrl Pts',(-20.2634348543251,25.7101873815761,-53.8551021690538));
#67754=CARTESIAN_POINT('Ctrl Pts',(-20.1997208256133,25.6132324220884,-53.8609556173536));
#67755=CARTESIAN_POINT('Ctrl Pts',(-20.1403262772436,25.5134952990801,-53.8668090656534));
#67756=CARTESIAN_POINT('Ctrl Pts',(-20.0854860496932,25.4114033115082,-53.8726625139532));
#67757=CARTESIAN_POINT('Ctrl Pts',(-20.0305834568958,25.3091952231778,-53.8785226188947));
#67758=CARTESIAN_POINT('Ctrl Pts',(-19.9802457182821,25.2046272894767,-53.8843827238362));
#67759=CARTESIAN_POINT('Ctrl Pts',(-19.9346607822561,25.0981495894455,-53.8902428287778));
#67760=CARTESIAN_POINT('Ctrl Pts',(-19.8890451476287,24.9916001833476,-53.8961068801332));
#67761=CARTESIAN_POINT('Ctrl Pts',(-19.8481888342136,24.8831388359249,-53.9019709314887));
#67762=CARTESIAN_POINT('Ctrl Pts',(-19.8122303096357,24.7732320357729,-53.9078349828442));
#67763=CARTESIAN_POINT('Ctrl Pts',(-19.7762187893704,24.6631632549366,-53.9137076766408));
#67764=CARTESIAN_POINT('Ctrl Pts',(-19.7451195750291,24.55164516638,-53.9195803704373));
#67765=CARTESIAN_POINT('Ctrl Pts',(-19.7190203566335,24.4391558002109,-53.9254530642339));
#67766=CARTESIAN_POINT('Ctrl Pts',(-19.7118748272236,24.4083580934721,-53.9270609095572));
#67767=CARTESIAN_POINT('Ctrl Pts',(-19.7051037844361,24.3774876172243,-53.9286687548805));
#67768=CARTESIAN_POINT('Ctrl Pts',(-19.6987083497125,24.3465542422555,-53.9302766002038));
#67769=CARTESIAN_POINT('Ctrl Pts',(-19.6753504486774,24.2335769791884,-53.9361488971725));
#67770=CARTESIAN_POINT('Ctrl Pts',(-19.6569285708432,24.1193818420497,-53.9420211941412));
#67771=CARTESIAN_POINT('Ctrl Pts',(-19.6435653853282,24.004438110966,-53.9478934911099));
#67772=CARTESIAN_POINT('Ctrl Pts',(-19.6302195174403,23.8896433378291,-53.9537581780481));
#67773=CARTESIAN_POINT('Ctrl Pts',(-19.6219193523074,23.7741023067914,-53.9596228649863));
#67774=CARTESIAN_POINT('Ctrl Pts',(-19.6187368359544,23.6582957367187,-53.9654875519245));
#67775=CARTESIAN_POINT('Ctrl Pts',(-19.6155575926203,23.5426082664538,-53.9713462073993));
#67776=CARTESIAN_POINT('Ctrl Pts',(-19.6174855406155,23.4266562110871,-53.9772048628741));
#67777=CARTESIAN_POINT('Ctrl Pts',(-19.6245408996489,23.3109260140997,-53.9830635183489));
#67778=CARTESIAN_POINT('Ctrl Pts',(-19.6318718472204,23.1906752936839,-53.9891510180668));
#67779=CARTESIAN_POINT('Ctrl Pts',(-19.6447389866202,23.0706645685832,-53.9952385177847));
#67780=CARTESIAN_POINT('Ctrl Pts',(-19.6631053345511,22.9514406515997,-54.0013260175026));
#67781=CARTESIAN_POINT('Ctrl Pts',(-19.6807607738904,22.8368315501046,-54.007177887586));
#67782=CARTESIAN_POINT('Ctrl Pts',(-19.703497551674,22.7229499258041,-54.0130297576694));
#67783=CARTESIAN_POINT('Ctrl Pts',(-19.7312299723037,22.6102761006779,-54.0188816277528));
#67784=CARTESIAN_POINT('Ctrl Pts',(-19.7589581704201,22.4976194311662,-54.0247326068358));
#67785=CARTESIAN_POINT('Ctrl Pts',(-19.7916804002322,22.3861705964729,-54.0305835859187));
#67786=CARTESIAN_POINT('Ctrl Pts',(-19.8292601733621,22.2763981957381,-54.0364345650017));
#67787=CARTESIAN_POINT('Ctrl Pts',(-19.8668433252753,22.1666159254079,-54.042286070144));
#67788=CARTESIAN_POINT('Ctrl Pts',(-19.909284754807,22.0585107797916,-54.0481375752863));
#67789=CARTESIAN_POINT('Ctrl Pts',(-19.9563988098579,21.9525340251846,-54.0539890804286));
#67790=CARTESIAN_POINT('Ctrl Pts',(-20.0035285104608,21.8465220780046,-54.0598425287283));
#67791=CARTESIAN_POINT('Ctrl Pts',(-20.055333754154,21.7426403047825,-54.0656959770281));
#67792=CARTESIAN_POINT('Ctrl Pts',(-20.1115819883891,21.6413172539527,-54.0715494253279));
#67793=CARTESIAN_POINT('Ctrl Pts',(-20.1678941890807,21.5398789768122,-54.0774095302694));
#67794=CARTESIAN_POINT('Ctrl Pts',(-20.228659264481,21.4410055916228,-54.083269635211));
#67795=CARTESIAN_POINT('Ctrl Pts',(-20.2936001496216,21.3450985093319,-54.0891297401525));
#67796=CARTESIAN_POINT('Ctrl Pts',(-20.3585847683837,21.2491268396237,-54.0949937915079));
#67797=CARTESIAN_POINT('Ctrl Pts',(-20.4277505503387,21.1561257813653,-54.1008578428634));
#67798=CARTESIAN_POINT('Ctrl Pts',(-20.5007798784254,21.0664639865547,-54.1067218942188));
#67799=CARTESIAN_POINT('Ctrl Pts',(-20.5739168371637,20.9766700481569,-54.1125945880154));
#67800=CARTESIAN_POINT('Ctrl Pts',(-20.6509284324033,20.8902255028893,-54.118467281812));
#67801=CARTESIAN_POINT('Ctrl Pts',(-20.7314598895681,20.807462521377,-54.1243399756085));
#67802=CARTESIAN_POINT('Ctrl Pts',(-20.7535080554138,20.7848034014938,-54.1259478209319));
#67803=CARTESIAN_POINT('Ctrl Pts',(-20.7758198693633,20.7624200084848,-54.1275556662553));
#67804=CARTESIAN_POINT('Ctrl Pts',(-20.7983876331438,20.7403186214169,-54.1291635115787));
#67805=CARTESIAN_POINT('Ctrl Pts',(-20.8808113644017,20.6595982272373,-54.1350358085474));
#67806=CARTESIAN_POINT('Ctrl Pts',(-20.9669278433428,20.5823722796293,-54.1409081055161));
#67807=CARTESIAN_POINT('Ctrl Pts',(-21.0564085645817,20.5089976479831,-54.1467804024848));
#67808=CARTESIAN_POINT('Ctrl Pts',(-21.1457733259119,20.4357181040326,-54.152645089423));
#67809=CARTESIAN_POINT('Ctrl Pts',(-21.2384933427765,20.3662802104363,-54.1585097763612));
#67810=CARTESIAN_POINT('Ctrl Pts',(-21.3342030682045,20.3010043455183,-54.1643744632994));
#67811=CARTESIAN_POINT('Ctrl Pts',(-21.4298143621718,20.235795612741,-54.1702331187742));
#67812=CARTESIAN_POINT('Ctrl Pts',(-21.5284089094472,20.1747406262545,-54.176091774249));
#67813=CARTESIAN_POINT('Ctrl Pts',(-21.6295883865782,20.1181193405628,-54.1819504297239));
#67814=CARTESIAN_POINT('Ctrl Pts',(-21.7347200232035,20.0592863775806,-54.1880379294418));
#67815=CARTESIAN_POINT('Ctrl Pts',(-21.8426422941227,20.0052408333132,-54.1941254291597));
#67816=CARTESIAN_POINT('Ctrl Pts',(-21.9528751655106,19.9562471685924,-54.2002129288776));
#67817=CARTESIAN_POINT('Ctrl Pts',(-22.0588412389685,19.9091499079531,-54.206064798961));
#67818=CARTESIAN_POINT('Ctrl Pts',(-22.1669419524992,19.8667208948666,-54.2119166690444));
#67819=CARTESIAN_POINT('Ctrl Pts',(-22.2767268810583,19.8291476665806,-54.2177685391278));
#67820=CARTESIAN_POINT('Ctrl Pts',(-22.3864950938636,19.7915801591602,-54.2236195182108));
#67821=CARTESIAN_POINT('Ctrl Pts',(-22.4979466208144,19.7588671003197,-54.2294704972937));
#67822=CARTESIAN_POINT('Ctrl Pts',(-22.6106134438374,19.7311469577971,-54.2353214763767));
#67823=CARTESIAN_POINT('Ctrl Pts',(-22.7232903966919,19.703424322967,-54.241172981519));
#67824=CARTESIAN_POINT('Ctrl Pts',(-22.8371824613953,19.6806955956169,-54.2470244866612));
#67825=CARTESIAN_POINT('Ctrl Pts',(-22.9518096272116,19.6630485120839,-54.2528759918035));
#67826=CARTESIAN_POINT('Ctrl Pts',(-23.0664748582145,19.6453955683386,-54.2587294401033));
#67827=CARTESIAN_POINT('Ctrl Pts',(-23.1818752673766,19.6328276867715,-54.264582888403));
#67828=CARTESIAN_POINT('Ctrl Pts',(-23.2975246051989,19.6253808656178,-54.2704363367028));
#67829=CARTESIAN_POINT('Ctrl Pts',(-23.4133054614312,19.6179255758114,-54.2762964416444));
#67830=CARTESIAN_POINT('Ctrl Pts',(-23.5293353985815,19.615602997042,-54.2821565465859));
#67831=CARTESIAN_POINT('Ctrl Pts',(-23.6451269375236,19.6183970095369,-54.2880166515274));
#67832=CARTESIAN_POINT('Ctrl Pts',(-23.7609964548192,19.6211929036244,-54.2938807028829));
#67833=CARTESIAN_POINT('Ctrl Pts',(-23.8766268428183,19.6291122218803,-54.2997447542383));
#67834=CARTESIAN_POINT('Ctrl Pts',(-23.9915362629233,19.6420870197753,-54.3056088055937));
#67835=CARTESIAN_POINT('Ctrl Pts',(-24.1066150365761,19.6550809399324,-54.3114814993902));
#67836=CARTESIAN_POINT('Ctrl Pts',(-24.220970314878,19.6731451457655,-54.3173541931868));
#67837=CARTESIAN_POINT('Ctrl Pts',(-24.3341308664104,19.6961607117757,-54.3232268869834));
#67838=CARTESIAN_POINT('Ctrl Pts',(-24.3651123324764,19.7024619887462,-54.3248347323068));
#67839=CARTESIAN_POINT('Ctrl Pts',(-24.3960043378739,19.7091341193543,-54.3264425776302));
#67840=CARTESIAN_POINT('Ctrl Pts',(-24.4267974386757,19.7161740210159,-54.3280504229536));
#67841=CARTESIAN_POINT('Ctrl Pts',(-24.5392623815807,19.7418856940145,-54.3339227199223));
#67842=CARTESIAN_POINT('Ctrl Pts',(-24.6507834746237,19.7725930341088,-54.339795016891));
#67843=CARTESIAN_POINT('Ctrl Pts',(-24.7608829065119,19.8082125672405,-54.3456673138597));
#67844=CARTESIAN_POINT('Ctrl Pts',(-24.8708396582798,19.843785940286,-54.3515320007979));
#67845=CARTESIAN_POINT('Ctrl Pts',(-24.9793780230043,19.8842587209834,-54.3573966877361));
#67846=CARTESIAN_POINT('Ctrl Pts',(-25.0860308673914,19.9294965465989,-54.3632613746743));
#67847=CARTESIAN_POINT('Ctrl Pts',(-25.1925740260051,19.974687847943,-54.3691200301491));
#67848=CARTESIAN_POINT('Ctrl Pts',(-25.2972351430538,20.024634286309,-54.3749786856239));
#67849=CARTESIAN_POINT('Ctrl Pts',(-25.3995633774041,20.0791520727706,-54.3808373410988));
#67850=CARTESIAN_POINT('Ctrl Pts',(-25.5058886427174,20.1357993719899,-54.3869248408167));
#67851=CARTESIAN_POINT('Ctrl Pts',(-25.6096946284807,20.1973822814309,-54.3930123405346));
#67852=CARTESIAN_POINT('Ctrl Pts',(-25.7104993607264,20.2636398928734,-54.3990998402525));
#67853=CARTESIAN_POINT('Ctrl Pts',(-25.8074022312365,20.3273328624284,-54.4049517103359));
#67854=CARTESIAN_POINT('Ctrl Pts',(-25.9015314902085,20.3953451261955,-54.4108035804193));
#67855=CARTESIAN_POINT('Ctrl Pts',(-25.9924858855782,20.4673991058602,-54.4166554505027));
#67856=CARTESIAN_POINT('Ctrl Pts',(-26.0834264323143,20.5394421146514,-54.4225064295857));
#67857=CARTESIAN_POINT('Ctrl Pts',(-26.1711927526675,20.6155253591283,-54.4283574086687));
#67858=CARTESIAN_POINT('Ctrl Pts',(-26.255415367797,20.6953299355161,-54.4342083877517));
#67859=CARTESIAN_POINT('Ctrl Pts',(-26.3396455553504,20.7751416871035,-54.440059892894));
#67860=CARTESIAN_POINT('Ctrl Pts',(-26.4203311042185,20.8586751513766,-54.4459113980363));
#67861=CARTESIAN_POINT('Ctrl Pts',(-26.4971387341967,20.9455739124591,-54.4517629031787));
#67862=CARTESIAN_POINT('Ctrl Pts',(-26.5739718703161,21.0325015307277,-54.4576163514784));
#67863=CARTESIAN_POINT('Ctrl Pts',(-26.6469242532682,21.1227963583951,-54.4634697997782));
#67864=CARTESIAN_POINT('Ctrl Pts',(-26.7157027586656,21.2160687641715,-54.4693232480779));
#67865=CARTESIAN_POINT('Ctrl Pts',(-26.7845594801588,21.3094472409272,-54.4751833530195));
#67866=CARTESIAN_POINT('Ctrl Pts',(-26.8492326045341,21.4058097215448,-54.481043457961));
#67867=CARTESIAN_POINT('Ctrl Pts',(-26.9094721904934,21.504737368236,-54.4869035629026));
#67868=CARTESIAN_POINT('Ctrl Pts',(-26.9697523440433,21.6037316365053,-54.492767614258));
#67869=CARTESIAN_POINT('Ctrl Pts',(-27.0255928153559,21.7052941492456,-54.4986316656134));
#67870=CARTESIAN_POINT('Ctrl Pts',(-27.0767903131154,21.8089828006621,-54.5044957169689));
#67871=CARTESIAN_POINT('Ctrl Pts',(-27.128063265767,21.9128242684532,-54.5103684107655));
#67872=CARTESIAN_POINT('Ctrl Pts',(-27.1746794221004,22.0187977518191,-54.5162411045621));
#67873=CARTESIAN_POINT('Ctrl Pts',(-27.2164841155747,22.1264425115873,-54.5221137983587));
#67874=CARTESIAN_POINT('Ctrl Pts',(-27.2279295413405,22.1559138461338,-54.5237216436819));
#67875=CARTESIAN_POINT('Ctrl Pts',(-27.2390146044347,22.1855103780317,-54.5253294890052));
#67876=CARTESIAN_POINT('Ctrl Pts',(-27.2497367934444,22.2152224956791,-54.5269373343285));
#67877=CARTESIAN_POINT('Ctrl Pts',(-27.2951872236293,22.3411695879713,-54.5337528513416));
#67878=CARTESIAN_POINT('Ctrl Pts',(-27.3342388739079,22.469541534013,-54.5405683683548));
#67879=CARTESIAN_POINT('Ctrl Pts',(-27.3666634540376,22.5997281123246,-54.547383885368));
#67880=CARTESIAN_POINT('Ctrl Pts',(-27.3989473711172,22.7293499202949,-54.5541698355708));
#67881=CARTESIAN_POINT('Ctrl Pts',(-27.4246614926118,22.8607705276024,-54.5609557857736));
#67882=CARTESIAN_POINT('Ctrl Pts',(-27.4436271962016,22.9933658989116,-54.5677417359765));
#67883=CARTESIAN_POINT('Ctrl Pts',(-27.4624434598956,23.1249164875493,-54.5744742164155));
#67884=CARTESIAN_POINT('Ctrl Pts',(-27.4746171475041,23.2576232611374,-54.5812066968546));
#67885=CARTESIAN_POINT('Ctrl Pts',(-27.4800212497374,23.3908573539461,-54.5879391772936));
#67886=CARTESIAN_POINT('Ctrl Pts',(-27.4821342678033,23.4429522316802,-54.5905715947022));
#67887=CARTESIAN_POINT('Ctrl Pts',(-27.4832128530943,23.4951275274992,-54.5932040121107));
#67888=CARTESIAN_POINT('Ctrl Pts',(-27.4832514569032,23.5473449030032,-54.5958364295193));
#67889=CARTESIAN_POINT('',(-27.4785230664524,23.5528363097046,-55.8458364779651));
#67890=CARTESIAN_POINT('Ctrl Pts',(-27.4791444786054,23.5473488992339,-54.595836477965));
#67891=CARTESIAN_POINT('Ctrl Pts',(-27.4732958893268,24.4059475501821,-54.6391657338778));
#67892=CARTESIAN_POINT('Ctrl Pts',(-26.7733364796375,26.5869150425722,-54.7487906269156));
#67893=CARTESIAN_POINT('Ctrl Pts',(-23.1677904881242,28.1864658159741,-54.9247111570782));
#67894=CARTESIAN_POINT('Ctrl Pts',(-19.4429915598308,25.7345506205814,-55.123598068453));
#67895=CARTESIAN_POINT('Ctrl Pts',(-19.4924172263766,21.2754506794386,-55.3224849798281));
#67896=CARTESIAN_POINT('Ctrl Pts',(-23.2706494908114,18.9067007691274,-55.5213718912028));
#67897=CARTESIAN_POINT('Ctrl Pts',(-26.810029366777,20.5717473545874,-55.6958223905819));
#67898=CARTESIAN_POINT('Ctrl Pts',(-27.4735450541292,22.7230378512852,-55.803977252836));
#67899=CARTESIAN_POINT('Ctrl Pts',(-27.4785230664524,23.5528363097046,-55.8458364779651));
#67900=CARTESIAN_POINT('',(-27.4885926759417,23.5521866781829,-57.095836477965));
#67901=CARTESIAN_POINT('Ctrl Pts',(-27.4785230664524,23.5528363097046,-55.8458364779651));
#67902=CARTESIAN_POINT('Ctrl Pts',(-27.4814291106918,24.0372527541313,-55.8702728899609));
#67903=CARTESIAN_POINT('Ctrl Pts',(-27.1735715217939,25.832320235274,-55.9610049390818));
#67904=CARTESIAN_POINT('Ctrl Pts',(-24.4862566433993,28.1070767695796,-56.1180326253275));
#67905=CARTESIAN_POINT('Ctrl Pts',(-20.2224697472459,26.8008851734482,-56.3169195367025));
#67906=CARTESIAN_POINT('Ctrl Pts',(-19.0166330805488,22.5076377877433,-56.5158064480773));
#67907=CARTESIAN_POINT('Ctrl Pts',(-21.9768083019133,19.1724649525765,-56.7146933594523));
#67908=CARTESIAN_POINT('Ctrl Pts',(-26.2600360440162,19.840941083895,-56.9080367027482));
#67909=CARTESIAN_POINT('Ctrl Pts',(-27.4813781435483,22.3557441605591,-57.035084408919));
#67910=CARTESIAN_POINT('Ctrl Pts',(-27.4885926759417,23.5521866781829,-57.095836477965));
#67911=CARTESIAN_POINT('',(-27.4832509534939,23.5467291638537,-58.345836477965));
#67912=CARTESIAN_POINT('Ctrl Pts',(-27.4885926759417,23.5521866781829,-57.095836477965));
#67913=CARTESIAN_POINT('Ctrl Pts',(-27.4892509951086,23.6613609113114,-57.101380046044));
#67914=CARTESIAN_POINT('Ctrl Pts',(-27.435543248894,25.0754943551076,-57.1732192512479));
#67915=CARTESIAN_POINT('Ctrl Pts',(-25.7292630861362,27.6603211242788,-57.3113540935769));
#67916=CARTESIAN_POINT('Ctrl Pts',(-21.2702304444974,27.6051569835892,-57.5102410049518));
#67917=CARTESIAN_POINT('Ctrl Pts',(-18.9063447869989,23.8238794508129,-57.7091279163267));
#67918=CARTESIAN_POINT('Ctrl Pts',(-20.8098166084289,19.7911619791023,-57.9080148277016));
#67919=CARTESIAN_POINT('Ctrl Pts',(-25.23151669269,19.2127300069044,-58.1069017390765));
#67920=CARTESIAN_POINT('Ctrl Pts',(-27.3424452633267,21.7130223291607,-58.2528422891643));
#67921=CARTESIAN_POINT('Ctrl Pts',(-27.4869488375757,23.2831178661222,-58.3324872021271));
#67922=CARTESIAN_POINT('Ctrl Pts',(-27.4845052556721,23.5467280401899,-58.345836477965));
#67923=CARTESIAN_POINT('',(-27.4832525204106,23.5499546106029,-59.5958364779354));
#67924=CARTESIAN_POINT('Ctrl Pts',(-27.4832509534939,23.5467291638537,-58.345836477965));
#67925=CARTESIAN_POINT('Ctrl Pts',(-27.4833531170139,23.6607703259115,-58.3516134412877));
#67926=CARTESIAN_POINT('Ctrl Pts',(-27.4784909918628,23.7749723276717,-58.3573904046104));
#67927=CARTESIAN_POINT('Ctrl Pts',(-27.4686493474181,23.8888605565914,-58.363167367933));
#67928=CARTESIAN_POINT('Ctrl Pts',(-27.4586046141927,24.0050989437275,-58.3690635426786));
#67929=CARTESIAN_POINT('Ctrl Pts',(-27.4433725210574,24.1210100185658,-58.3749597174241));
#67930=CARTESIAN_POINT('Ctrl Pts',(-27.4229929270286,24.2360883942338,-58.3808558921697));
#67931=CARTESIAN_POINT('Ctrl Pts',(-27.4030531299606,24.3486833485048,-58.3866248259246));
#67932=CARTESIAN_POINT('Ctrl Pts',(-27.3781858356613,24.4604807384687,-58.3923937596795));
#67933=CARTESIAN_POINT('Ctrl Pts',(-27.3484806902701,24.5710129616683,-58.3981626934344));
#67934=CARTESIAN_POINT('Ctrl Pts',(-27.3187822067082,24.681520396341,-58.4039303334184));
#67935=CARTESIAN_POINT('Ctrl Pts',(-27.2842481385667,24.790762816491,-58.4096979734024));
#67936=CARTESIAN_POINT('Ctrl Pts',(-27.2450187657923,24.8982849776571,-58.4154656133865));
#67937=CARTESIAN_POINT('Ctrl Pts',(-27.2057880539103,25.0058108091275,-58.4212334502508));
#67938=CARTESIAN_POINT('Ctrl Pts',(-27.1618618658653,25.111615864635,-58.4270012871151));
#67939=CARTESIAN_POINT('Ctrl Pts',(-27.113429356445,25.215263016814,-58.4327691239794));
#67940=CARTESIAN_POINT('Ctrl Pts',(-27.0631128439418,25.3229419971303,-58.4387613271333));
#67941=CARTESIAN_POINT('Ctrl Pts',(-27.0079325042467,25.4282913250685,-58.4447535302872));
#67942=CARTESIAN_POINT('Ctrl Pts',(-26.9481532417051,25.5308483422793,-58.4507457334411));
#67943=CARTESIAN_POINT('Ctrl Pts',(-26.8905314358294,25.6297040371419,-58.4565216756696));
#67944=CARTESIAN_POINT('Ctrl Pts',(-26.8286372096835,25.7259651579475,-58.4622976178982));
#67945=CARTESIAN_POINT('Ctrl Pts',(-26.7627516086389,25.8192476133614,-58.4680735601267));
#67946=CARTESIAN_POINT('Ctrl Pts',(-26.6968214320502,25.9125931799275,-58.473853410125));
#67947=CARTESIAN_POINT('Ctrl Pts',(-26.6268947686452,26.0029557362783,-58.4796332601234));
#67948=CARTESIAN_POINT('Ctrl Pts',(-26.5532921780326,26.0899851716624,-58.4854131101218));
#67949=CARTESIAN_POINT('Ctrl Pts',(-26.4795853896802,26.1771378129063,-58.4912011425402));
#67950=CARTESIAN_POINT('Ctrl Pts',(-26.4021925845177,26.2609476126844,-58.4969891749585));
#67951=CARTESIAN_POINT('Ctrl Pts',(-26.3214700984561,26.3411022585104,-58.5027772073768));
#67952=CARTESIAN_POINT('Ctrl Pts',(-26.3126449986922,26.3498652783388,-58.5034099921933));
#67953=CARTESIAN_POINT('Ctrl Pts',(-26.3037801325963,26.3585846517521,-58.5040427770098));
#67954=CARTESIAN_POINT('Ctrl Pts',(-26.294875988009,26.3672600011636,-58.5046755618263));
#67955=CARTESIAN_POINT('Ctrl Pts',(-26.2122447681908,26.447767982273,-58.510547858795));
#67956=CARTESIAN_POINT('Ctrl Pts',(-26.125929807076,26.5247720238348,-58.5164201557637));
#67957=CARTESIAN_POINT('Ctrl Pts',(-26.0362605274874,26.5979161031621,-58.5222924527324));
#67958=CARTESIAN_POINT('Ctrl Pts',(-25.9467074521637,26.6709653935715,-58.5281571396706));
#67959=CARTESIAN_POINT('Ctrl Pts',(-25.8538090202221,26.7401644104525,-58.5340218266088));
#67960=CARTESIAN_POINT('Ctrl Pts',(-25.7579316020259,26.8051937174024,-58.539886513547));
#67961=CARTESIAN_POINT('Ctrl Pts',(-25.6621527877523,26.8701561457809,-58.5457451690218));
#67962=CARTESIAN_POINT('Ctrl Pts',(-25.5634014211407,26.9309571632031,-58.5516038244966));
#67963=CARTESIAN_POINT('Ctrl Pts',(-25.4620765448829,26.9873178413145,-58.5574624799714));
#67964=CARTESIAN_POINT('Ctrl Pts',(-25.3567938297124,27.0458800171548,-58.5635499796894));
#67965=CARTESIAN_POINT('Ctrl Pts',(-25.2487328115532,27.0996476074849,-58.5696374794073));
#67966=CARTESIAN_POINT('Ctrl Pts',(-25.1383742033206,27.1483573878804,-58.5757249791252));
#67967=CARTESIAN_POINT('Ctrl Pts',(-25.0322872599303,27.1951817525414,-58.5815768492086));
#67968=CARTESIAN_POINT('Ctrl Pts',(-24.9240776988716,27.2373323908853,-58.587428719292));
#67969=CARTESIAN_POINT('Ctrl Pts',(-24.814196426388,27.2746229256086,-58.5932805893754));
#67970=CARTESIAN_POINT('Ctrl Pts',(-24.7043318843272,27.311907782509,-58.5991315684583));
#67971=CARTESIAN_POINT('Ctrl Pts',(-24.5927965282824,27.3443338743237,-58.6049825475413));
#67972=CARTESIAN_POINT('Ctrl Pts',(-24.4800587311707,27.3717639383781,-58.6108335266243));
#67973=CARTESIAN_POINT('Ctrl Pts',(-24.3673107978464,27.3991964686591,-58.6166850317666));
#67974=CARTESIAN_POINT('Ctrl Pts',(-24.2533606102291,27.4216319804953,-58.6225365369089));
#67975=CARTESIAN_POINT('Ctrl Pts',(-24.1386884032842,27.4389839733119,-58.6283880420511));
#67976=CARTESIAN_POINT('Ctrl Pts',(-24.0239781161958,27.4563417283476,-58.6342414903509));
#67977=CARTESIAN_POINT('Ctrl Pts',(-23.908545741532,27.4686125458159,-58.6400949386507));
#67978=CARTESIAN_POINT('Ctrl Pts',(-23.7928776198352,27.4757616791303,-58.6459483869504));
#67979=CARTESIAN_POINT('Ctrl Pts',(-23.6770779583671,27.4829189425617,-58.6518084918919));
#67980=CARTESIAN_POINT('Ctrl Pts',(-23.5610424275956,27.4849428708623,-58.6576685968335));
#67981=CARTESIAN_POINT('Ctrl Pts',(-23.4452584635423,27.4818508384459,-58.663528701775));
#67982=CARTESIAN_POINT('Ctrl Pts',(-23.329396526236,27.4787567237392,-58.6693927531304));
#67983=CARTESIAN_POINT('Ctrl Pts',(-23.2137869043208,27.4705398173157,-58.6752568044859));
#67984=CARTESIAN_POINT('Ctrl Pts',(-23.0989112599195,27.4572693036563,-58.6811208558413));
#67985=CARTESIAN_POINT('Ctrl Pts',(-22.9838663117496,27.4439792319087,-58.6869935496379));
#67986=CARTESIAN_POINT('Ctrl Pts',(-22.8695579066507,27.4256207534428,-58.6928662434344));
#67987=CARTESIAN_POINT('Ctrl Pts',(-22.7564569683847,27.4023140062387,-58.698738937231));
#67988=CARTESIAN_POINT('Ctrl Pts',(-22.725491823434,27.3959330087283,-58.7003467825544));
#67989=CARTESIAN_POINT('Ctrl Pts',(-22.6946170933743,27.3891813890662,-58.7019546278778));
#67990=CARTESIAN_POINT('Ctrl Pts',(-22.6638422141674,27.3820622541337,-58.7035624732012));
#67991=CARTESIAN_POINT('Ctrl Pts',(-22.5514438215795,27.3560611992588,-58.7094347701699));
#67992=CARTESIAN_POINT('Ctrl Pts',(-22.4400021337872,27.3250669231564,-58.7153070671386));
#67993=CARTESIAN_POINT('Ctrl Pts',(-22.3299947456515,27.2891641294191,-58.7211793641073));
#67994=CARTESIAN_POINT('Ctrl Pts',(-22.2201299183543,27.2533078628513,-58.7270440510455));
#67995=CARTESIAN_POINT('Ctrl Pts',(-22.1116960837057,27.2125558555647,-58.7329087379837));
#67996=CARTESIAN_POINT('Ctrl Pts',(-22.0051600276238,27.1670436721757,-58.7387734249219));
#67997=CARTESIAN_POINT('Ctrl Pts',(-21.8987335372064,27.1215782952182,-58.7446320803967));
#67998=CARTESIAN_POINT('Ctrl Pts',(-21.7942013210934,27.0713626410679,-58.7504907358715));
#67999=CARTESIAN_POINT('Ctrl Pts',(-21.6920137458813,27.0165816584363,-58.7563493913463));
#68000=CARTESIAN_POINT('Ctrl Pts',(-21.5858346339755,26.9596608823725,-58.7624368910642));
#68001=CARTESIAN_POINT('Ctrl Pts',(-21.4821874967579,26.897810996664,-58.7685243907821));
#68002=CARTESIAN_POINT('Ctrl Pts',(-21.3815536350633,26.8312941491919,-58.7746118905));
#68003=CARTESIAN_POINT('Ctrl Pts',(-21.284815021196,26.7673519778897,-58.7804637605834));
#68004=CARTESIAN_POINT('Ctrl Pts',(-21.1908611268622,26.6990976655215,-58.7863156306668));
#68005=CARTESIAN_POINT('Ctrl Pts',(-21.1000924883545,26.6268098222418,-58.7921675007502));
#68006=CARTESIAN_POINT('Ctrl Pts',(-21.0093376701973,26.5545329854436,-58.7980184798332));
#68007=CARTESIAN_POINT('Ctrl Pts',(-20.9217674668391,26.4782240963009,-58.8038694589162));
#68008=CARTESIAN_POINT('Ctrl Pts',(-20.8377505350885,26.3982030085125,-58.8097204379991));
#68009=CARTESIAN_POINT('Ctrl Pts',(-20.7537260494073,26.3181747260585,-58.8155719431414));
#68010=CARTESIAN_POINT('Ctrl Pts',(-20.6732557697725,26.234433866588,-58.8214234482837));
#68011=CARTESIAN_POINT('Ctrl Pts',(-20.5966720579262,26.1473377026072,-58.827274953426));
#68012=CARTESIAN_POINT('Ctrl Pts',(-20.5200629142958,26.0602126158858,-58.8331284017258));
#68013=CARTESIAN_POINT('Ctrl Pts',(-20.4473431776449,25.969730319366,-58.8389818500256));
#68014=CARTESIAN_POINT('Ctrl Pts',(-20.3788049685402,25.8762811975031,-58.8448352983254));
#68015=CARTESIAN_POINT('Ctrl Pts',(-20.3101888166095,25.7827258036972,-58.850695403267));
#68016=CARTESIAN_POINT('Ctrl Pts',(-20.2457639282949,25.6861971838331,-58.8565555082085));
#68017=CARTESIAN_POINT('Ctrl Pts',(-20.1857791660443,25.5871148176213,-58.86241561315));
#68018=CARTESIAN_POINT('Ctrl Pts',(-20.1257540078105,25.4879657256372,-58.8682796645055));
#68019=CARTESIAN_POINT('Ctrl Pts',(-20.0701751273649,25.3862598247315,-58.8741437158609));
#68020=CARTESIAN_POINT('Ctrl Pts',(-20.0192446774394,25.2824397424745,-58.8800077672164));
#68021=CARTESIAN_POINT('Ctrl Pts',(-19.9682391661974,25.1784666501408,-58.8858804610129));
#68022=CARTESIAN_POINT('Ctrl Pts',(-19.9218959233207,25.0723735351543,-58.8917531548095));
#68023=CARTESIAN_POINT('Ctrl Pts',(-19.8803684289681,24.9646215332487,-58.8976258486061));
#68024=CARTESIAN_POINT('Ctrl Pts',(-19.8689988956845,24.9351208375979,-58.8992336939294));
#68025=CARTESIAN_POINT('Ctrl Pts',(-19.8579900461171,24.9054958725272,-58.9008415392527));
#68026=CARTESIAN_POINT('Ctrl Pts',(-19.8473443669317,24.8757562560705,-58.902449384576));
#68027=CARTESIAN_POINT('Ctrl Pts',(-19.8084633945502,24.7671389301154,-58.9083216815447));
#68028=CARTESIAN_POINT('Ctrl Pts',(-19.7743004424646,24.6566274482055,-58.9141939785134));
#68029=CARTESIAN_POINT('Ctrl Pts',(-19.7450424083901,24.5446694047933,-58.9200662754821));
#68030=CARTESIAN_POINT('Ctrl Pts',(-19.7158222904042,24.432856450114,-58.9259309624203));
#68031=CARTESIAN_POINT('Ctrl Pts',(-19.6914945534176,24.3196010581559,-58.9317956493585));
#68032=CARTESIAN_POINT('Ctrl Pts',(-19.6721974622212,24.2053692221658,-58.9376603362967));
#68033=CARTESIAN_POINT('Ctrl Pts',(-19.652920216875,24.0912548664679,-58.9435189917715));
#68034=CARTESIAN_POINT('Ctrl Pts',(-19.6386633949981,23.9761664693238,-58.9493776472463));
#68035=CARTESIAN_POINT('Ctrl Pts',(-19.629514838374,23.8605829043263,-58.9552363027212));
#68036=CARTESIAN_POINT('Ctrl Pts',(-19.6200089310701,23.7404845434751,-58.9613238024391));
#68037=CARTESIAN_POINT('Ctrl Pts',(-19.6160186060692,23.6198519826886,-58.967411302157));
#68038=CARTESIAN_POINT('Ctrl Pts',(-19.6175834774655,23.4992318504771,-58.9734988018749));
#68039=CARTESIAN_POINT('Ctrl Pts',(-19.6190877771834,23.3832805772363,-58.9793506719583));
#68040=CARTESIAN_POINT('Ctrl Pts',(-19.6257252124908,23.2673412402109,-58.9852025420417));
#68041=CARTESIAN_POINT('Ctrl Pts',(-19.6374778908361,23.1519014179038,-58.9910544121251));
#68042=CARTESIAN_POINT('Ctrl Pts',(-19.6492287797293,23.0364791723595,-58.996905391208));
#68043=CARTESIAN_POINT('Ctrl Pts',(-19.6660933212149,22.9215567014546,-59.002756370291));
#68044=CARTESIAN_POINT('Ctrl Pts',(-19.6880016916431,22.8076170568317,-59.008607349374));
#68045=CARTESIAN_POINT('Ctrl Pts',(-19.7099120318445,22.6936671679382,-59.0144588545163));
#68046=CARTESIAN_POINT('Ctrl Pts',(-19.7368670244221,22.5807006869601,-59.0203103596586));
#68047=CARTESIAN_POINT('Ctrl Pts',(-19.7687457456332,22.4691903563431,-59.0261618648009));
#68048=CARTESIAN_POINT('Ctrl Pts',(-19.8006350530737,22.3576429955728,-59.0320153131006));
#68049=CARTESIAN_POINT('Ctrl Pts',(-19.8374512268016,22.2475531439335,-59.0378687614004));
#68050=CARTESIAN_POINT('Ctrl Pts',(-19.8790237333752,22.1393775867069,-59.0437222097002));
#68051=CARTESIAN_POINT('Ctrl Pts',(-19.9206435169159,22.031079010382,-59.0495823146417));
#68052=CARTESIAN_POINT('Ctrl Pts',(-19.9670302810896,21.924699459731,-59.0554424195833));
#68053=CARTESIAN_POINT('Ctrl Pts',(-20.017965631281,21.8206750534733,-59.0613025245248));
#68054=CARTESIAN_POINT('Ctrl Pts',(-20.0689352832428,21.7165805932883,-59.0671665758803));
#68055=CARTESIAN_POINT('Ctrl Pts',(-20.1244594230848,21.6148447975942,-59.0730306272357));
#68056=CARTESIAN_POINT('Ctrl Pts',(-20.184274932927,21.5158769998424,-59.0788946785912));
#68057=CARTESIAN_POINT('Ctrl Pts',(-20.2441785988902,21.4167633433127,-59.0847673723878));
#68058=CARTESIAN_POINT('Ctrl Pts',(-20.3083860291805,21.3204261692656,-59.0906400661843));
#68059=CARTESIAN_POINT('Ctrl Pts',(-20.3765922251004,21.2272438665465,-59.0965127599809));
#68060=CARTESIAN_POINT('Ctrl Pts',(-20.3952659405929,21.2017321108117,-59.0981206053042));
#68061=CARTESIAN_POINT('Ctrl Pts',(-20.4142391708724,21.1764566314493,-59.0997284506276));
#68062=CARTESIAN_POINT('Ctrl Pts',(-20.433505168274,21.1514247194882,-59.1013362959509));
#68063=CARTESIAN_POINT('Ctrl Pts',(-20.5038699331547,21.0600012357751,-59.1072085929196));
#68064=CARTESIAN_POINT('Ctrl Pts',(-20.5783785732018,20.9715232301045,-59.1130808898883));
#68065=CARTESIAN_POINT('Ctrl Pts',(-20.6567555458308,20.8863898864365,-59.118953186857));
#68066=CARTESIAN_POINT('Ctrl Pts',(-20.7350309481279,20.8013668688207,-59.1248178737952));
#68067=CARTESIAN_POINT('Ctrl Pts',(-20.817164436442,20.7196801949267,-59.1306825607334));
#68068=CARTESIAN_POINT('Ctrl Pts',(-20.9028387008172,20.6416980783478,-59.1365472476716));
#68069=CARTESIAN_POINT('Ctrl Pts',(-20.9884248545749,20.5637961614939,-59.1424059031464));
#68070=CARTESIAN_POINT('Ctrl Pts',(-21.07754423746,20.4895915004444,-59.1482645586213));
#68071=CARTESIAN_POINT('Ctrl Pts',(-21.1698414472921,20.4194168494433,-59.1541232140961));
#68072=CARTESIAN_POINT('Ctrl Pts',(-21.2657438674344,20.3465011147652,-59.160210713814));
#68073=CARTESIAN_POINT('Ctrl Pts',(-21.3650771250021,20.277936974309,-59.1662982135319));
#68074=CARTESIAN_POINT('Ctrl Pts',(-21.4674027453553,20.2140532319599,-59.1723857132498));
#68075=CARTESIAN_POINT('Ctrl Pts',(-21.5657676347611,20.1526422458421,-59.1782375833332));
#68076=CARTESIAN_POINT('Ctrl Pts',(-21.6668971594238,20.0955563048513,-59.1840894534166));
#68077=CARTESIAN_POINT('Ctrl Pts',(-21.7703714396855,20.0430439125343,-59.1899413235));
#68078=CARTESIAN_POINT('Ctrl Pts',(-21.8738299650472,19.9905395157064,-59.195792302583));
#68079=CARTESIAN_POINT('Ctrl Pts',(-21.9796321676288,19.9426074699822,-59.201643281666));
#68080=CARTESIAN_POINT('Ctrl Pts',(-22.0873339053358,19.8994501414444,-59.207494260749));
#68081=CARTESIAN_POINT('Ctrl Pts',(-22.1950453264651,19.8562889326476,-59.2133457658912));
#68082=CARTESIAN_POINT('Ctrl Pts',(-22.3046562384826,19.817903448203,-59.2191972710335));
#68083=CARTESIAN_POINT('Ctrl Pts',(-22.4157035508278,19.7844474902701,-59.2250487761758));
#68084=CARTESIAN_POINT('Ctrl Pts',(-22.5267877395681,19.7509804223419,-59.2309022244756));
#68085=CARTESIAN_POINT('Ctrl Pts',(-22.6393088815149,19.722446255159,-59.2367556727753));
#68086=CARTESIAN_POINT('Ctrl Pts',(-22.7527904949922,19.6989484278848,-59.2426091210751));
#68087=CARTESIAN_POINT('Ctrl Pts',(-22.8664011617061,19.6754238784785,-59.2484692260166));
#68088=CARTESIAN_POINT('Ctrl Pts',(-22.9809740750415,19.6569471845903,-59.2543293309582));
#68089=CARTESIAN_POINT('Ctrl Pts',(-23.0960242694544,19.6435703478222,-59.2601894358997));
#68090=CARTESIAN_POINT('Ctrl Pts',(-23.2111519429727,19.6301845025918,-59.2660534872552));
#68091=CARTESIAN_POINT('Ctrl Pts',(-23.3267571262581,19.6219053825794,-59.2719175386106));
#68092=CARTESIAN_POINT('Ctrl Pts',(-23.4423532138419,19.6187328843813,-59.2777815899661));
#68093=CARTESIAN_POINT('Ctrl Pts',(-23.5581196669834,19.6155557105542,-59.2836542837626));
#68094=CARTESIAN_POINT('Ctrl Pts',(-23.6738765858963,19.6175001723504,-59.2895269775592));
#68095=CARTESIAN_POINT('Ctrl Pts',(-23.7891407609701,19.6245142044603,-59.2953996713558));
#68096=CARTESIAN_POINT('Ctrl Pts',(-23.8206981639717,19.6264345291216,-59.2970075166791));
#68097=CARTESIAN_POINT('Ctrl Pts',(-23.8522186841367,19.6287345579943,-59.2986153620025));
#68098=CARTESIAN_POINT('Ctrl Pts',(-23.883692540001,19.6314125552649,-59.3002232073259));
#68099=CARTESIAN_POINT('Ctrl Pts',(-23.9986437891668,19.641193343893,-59.3060955042946));
#68100=CARTESIAN_POINT('Ctrl Pts',(-24.1133568984343,19.6560525999751,-59.3119678012633));
#68101=CARTESIAN_POINT('Ctrl Pts',(-24.2273470851922,19.675974280765,-59.317840098232));
#68102=CARTESIAN_POINT('Ctrl Pts',(-24.341189549721,19.6958701446386,-59.3237047851702));
#68103=CARTESIAN_POINT('Ctrl Pts',(-24.4543105513467,19.7208153162297,-59.3295694721084));
#68104=CARTESIAN_POINT('Ctrl Pts',(-24.5662287863124,19.750741872405,-59.3354341590466));
#68105=CARTESIAN_POINT('Ctrl Pts',(-24.6780319203796,19.7806376509907,-59.3412928145214));
#68106=CARTESIAN_POINT('Ctrl Pts',(-24.7886343512326,19.8155045180228,-59.3471514699962));
#68107=CARTESIAN_POINT('Ctrl Pts',(-24.8975640171979,19.8552233354591,-59.353010125471));
#68108=CARTESIAN_POINT('Ctrl Pts',(-25.0107485718599,19.8964936048884,-59.3590976251889));
#68109=CARTESIAN_POINT('Ctrl Pts',(-25.1221265703629,19.9430025165613,-59.3651851249068));
#68110=CARTESIAN_POINT('Ctrl Pts',(-25.2311843703503,19.9945589068451,-59.3712726246247));
#68111=CARTESIAN_POINT('Ctrl Pts',(-25.3360208560475,20.0441196972996,-59.3771244947081));
#68112=CARTESIAN_POINT('Ctrl Pts',(-25.4387130112703,20.0983442920242,-59.3829763647915));
#68113=CARTESIAN_POINT('Ctrl Pts',(-25.5388248030602,20.1570137659198,-59.3888282348749));
#68114=CARTESIAN_POINT('Ctrl Pts',(-25.6389213519195,20.2156743068545,-59.3946792139579));
#68115=CARTESIAN_POINT('Ctrl Pts',(-25.7364379619719,20.2787781723643,-59.4005301930409));
#68116=CARTESIAN_POINT('Ctrl Pts',(-25.8309643016064,20.3460610856998,-59.4063811721238));
#68117=CARTESIAN_POINT('Ctrl Pts',(-25.9254991400683,20.4133500484165,-59.4122326772661));
#68118=CARTESIAN_POINT('Ctrl Pts',(-26.0170428368545,20.4848185661572,-59.4180841824084));
#68119=CARTESIAN_POINT('Ctrl Pts',(-26.105215675548,20.560160169651,-59.4239356875507));
#68120=CARTESIAN_POINT('Ctrl Pts',(-26.1934177945225,20.6355267924519,-59.4297891358505));
#68121=CARTESIAN_POINT('Ctrl Pts',(-26.2782465154595,20.7147687900684,-59.4356425841503));
#68122=CARTESIAN_POINT('Ctrl Pts',(-26.3593572547097,20.7975412037247,-59.4414960324501));
#68123=CARTESIAN_POINT('Ctrl Pts',(-26.4405602344828,20.8804077475884,-59.4473561373916));
#68124=CARTESIAN_POINT('Ctrl Pts',(-26.5180365038056,20.9668124255809,-59.4532162423331));
#68125=CARTESIAN_POINT('Ctrl Pts',(-26.5914801684225,21.0563753371235,-59.4590763472746));
#68126=CARTESIAN_POINT('Ctrl Pts',(-26.6649732927511,21.1459985636818,-59.4649403986301));
#68127=CARTESIAN_POINT('Ctrl Pts',(-26.7344281577441,21.2387839286889,-59.4708044499856));
#68128=CARTESIAN_POINT('Ctrl Pts',(-26.7995818195121,21.3343219869053,-59.476668501341));
#68129=CARTESIAN_POINT('Ctrl Pts',(-26.8648315047715,21.4300008491479,-59.4825411951376));
#68130=CARTESIAN_POINT('Ctrl Pts',(-26.9257671183942,21.5284401512598,-59.4884138889341));
#68131=CARTESIAN_POINT('Ctrl Pts',(-26.9821712685195,21.6292052173816,-59.4942865827307));
#68132=CARTESIAN_POINT('Ctrl Pts',(-26.9976137812974,21.6567930068918,-59.495894428054));
#68133=CARTESIAN_POINT('Ctrl Pts',(-27.0127169058148,21.6845550124757,-59.4975022733773));
#68134=CARTESIAN_POINT('Ctrl Pts',(-27.0274768151446,21.7124820665429,-59.4991101187007));
#68135=CARTESIAN_POINT('Ctrl Pts',(-27.0845220828676,21.8204167591193,-59.5053242467739));
#68136=CARTESIAN_POINT('Ctrl Pts',(-27.1366100965118,21.9311458948516,-59.5115383748472));
#68137=CARTESIAN_POINT('Ctrl Pts',(-27.1834742626248,22.0442017842446,-59.5177525029205));
#68138=CARTESIAN_POINT('Ctrl Pts',(-27.2325471217173,22.1625859611095,-59.5242595008384));
#68139=CARTESIAN_POINT('Ctrl Pts',(-27.2758914982486,22.2835212836231,-59.5307664987563));
#68140=CARTESIAN_POINT('Ctrl Pts',(-27.3132539937852,22.4064391744103,-59.5372734966742));
#68141=CARTESIAN_POINT('Ctrl Pts',(-27.3487733347603,22.5232933195125,-59.5434594934726));
#68142=CARTESIAN_POINT('Ctrl Pts',(-27.3788866604174,22.6419387339928,-59.549645490271));
#68143=CARTESIAN_POINT('Ctrl Pts',(-27.4034243477068,22.7618643301806,-59.5558314870695));
#68144=CARTESIAN_POINT('Ctrl Pts',(-27.4279237226215,22.8816026783065,-59.5620078252467));
#68145=CARTESIAN_POINT('Ctrl Pts',(-27.4468647295695,23.00261689376,-59.5681841634239));
#68146=CARTESIAN_POINT('Ctrl Pts',(-27.4601275277268,23.1243810541338,-59.574360501601));
#68147=CARTESIAN_POINT('Ctrl Pts',(-27.4733643544789,23.2459067741507,-59.5805247451826));
#68148=CARTESIAN_POINT('Ctrl Pts',(-27.4809450984992,23.3681791729121,-59.5866889887642));
#68149=CARTESIAN_POINT('Ctrl Pts',(-27.482801082237,23.4906631230373,-59.5928532323458));
#68150=CARTESIAN_POINT('Ctrl Pts',(-27.4831004893595,23.5104222223859,-59.5938476475423));
#68151=CARTESIAN_POINT('Ctrl Pts',(-27.4832510230179,23.5301868073856,-59.5948420627388));
#68152=CARTESIAN_POINT('Ctrl Pts',(-27.4832525204106,23.5499546106029,-59.5958364779354));
#68153=CARTESIAN_POINT('',(-27.4832508599701,23.5538787940674,-60.8458364779651));
#68154=CARTESIAN_POINT('Ctrl Pts',(-27.4832525204106,23.5499546111917,-59.595836477965));
#68155=CARTESIAN_POINT('Ctrl Pts',(-27.4832616993984,23.6711310949174,-59.6019322355743));
#68156=CARTESIAN_POINT('Ctrl Pts',(-27.477666351959,23.7922129670324,-59.6080279931836));
#68157=CARTESIAN_POINT('Ctrl Pts',(-27.4665185564701,23.9126741414055,-59.6141237507928));
#68158=CARTESIAN_POINT('Ctrl Pts',(-27.4553574565759,24.0332790809115,-59.6202267834217));
#68159=CARTESIAN_POINT('Ctrl Pts',(-27.4386307271698,24.153261486616,-59.6263298160506));
#68160=CARTESIAN_POINT('Ctrl Pts',(-27.4164418763637,24.2721035905451,-59.6324328486795));
#68161=CARTESIAN_POINT('Ctrl Pts',(-27.3942034556774,24.391211187667,-59.6385495154798));
#68162=CARTESIAN_POINT('Ctrl Pts',(-27.366478591319,24.5091730359776,-59.6446661822801));
#68163=CARTESIAN_POINT('Ctrl Pts',(-27.333421517184,24.6254834032879,-59.6507828490804));
#68164=CARTESIAN_POINT('Ctrl Pts',(-27.3003247017988,24.7419335990474,-59.6569068693442));
#68165=CARTESIAN_POINT('Ctrl Pts',(-27.2618830036239,24.8567280117497,-59.6630308896079));
#68166=CARTESIAN_POINT('Ctrl Pts',(-27.2182993012072,24.9693796918406,-59.6691549098717));
#68167=CARTESIAN_POINT('Ctrl Pts',(-27.1746185298994,25.0822822678641,-59.6752925694507));
#68168=CARTESIAN_POINT('Ctrl Pts',(-27.1257730077416,25.19303224151,-59.6814302290296));
#68169=CARTESIAN_POINT('Ctrl Pts',(-27.0720127091686,25.3011649373717,-59.6875678886086));
#68170=CARTESIAN_POINT('Ctrl Pts',(-27.0415627875594,25.3624114743103,-59.6910442690976));
#68171=CARTESIAN_POINT('Ctrl Pts',(-27.0095369683429,25.4228188506372,-59.6945206495867));
#68172=CARTESIAN_POINT('Ctrl Pts',(-26.9759867937984,25.4823068180551,-59.6979970300757));
#68173=CARTESIAN_POINT('Ctrl Pts',(-26.9193138867624,25.582793807855,-59.7038693270444));
#68174=CARTESIAN_POINT('Ctrl Pts',(-26.8581209145749,25.6809534486651,-59.7097416240131));
#68175=CARTESIAN_POINT('Ctrl Pts',(-26.7926239578226,25.7763514816572,-59.7156139209819));
#68176=CARTESIAN_POINT('Ctrl Pts',(-26.7272118799245,25.8716258863749,-59.7214786079201));
#68177=CARTESIAN_POINT('Ctrl Pts',(-26.6575071411671,25.9641454626237,-59.7273432948583));
#68178=CARTESIAN_POINT('Ctrl Pts',(-26.5837715632439,26.0535006786476,-59.7332079817964));
#68179=CARTESIAN_POINT('Ctrl Pts',(-26.5101118177467,26.1427639984255,-59.7390666372713));
#68180=CARTESIAN_POINT('Ctrl Pts',(-26.4324297401534,26.2288691141159,-59.7449252927461));
#68181=CARTESIAN_POINT('Ctrl Pts',(-26.3510298926307,26.3114361863006,-59.7507839482209));
#68182=CARTESIAN_POINT('Ctrl Pts',(-26.2664504953678,26.3972284010489,-59.7568714479388));
#68183=CARTESIAN_POINT('Ctrl Pts',(-26.1778572258801,26.4792001645838,-59.7629589476567));
#68184=CARTESIAN_POINT('Ctrl Pts',(-26.0856374382027,26.556963754251,-59.7690464473746));
#68185=CARTESIAN_POINT('Ctrl Pts',(-25.9969872137074,26.6317173386517,-59.774898317458));
#68186=CARTESIAN_POINT('Ctrl Pts',(-25.9049863405209,26.7025821730215,-59.7807501875414));
#68187=CARTESIAN_POINT('Ctrl Pts',(-25.8100151660706,26.7692526615911,-59.7866020576248));
#68188=CARTESIAN_POINT('Ctrl Pts',(-25.7150584518453,26.8359129989724,-59.7924530367077));
#68189=CARTESIAN_POINT('Ctrl Pts',(-25.6171326738288,26.898380022899,-59.7983040157907));
#68190=CARTESIAN_POINT('Ctrl Pts',(-25.5166487461557,26.9563903632788,-59.8041549948736));
#68191=CARTESIAN_POINT('Ctrl Pts',(-25.4161557840106,27.0144059193463,-59.8100065000159));
#68192=CARTESIAN_POINT('Ctrl Pts',(-25.3131045730134,27.0679637886221,-59.8158580051582));
#68193=CARTESIAN_POINT('Ctrl Pts',(-25.2079316783369,27.1168459829844,-59.8217095103005));
#68194=CARTESIAN_POINT('Ctrl Pts',(-25.1027238580312,27.1657444100595,-59.8275629586003));
#68195=CARTESIAN_POINT('Ctrl Pts',(-24.9953933277361,27.2099639006548,-59.8334164069));
#68196=CARTESIAN_POINT('Ctrl Pts',(-24.8863970580109,27.2493344184323,-59.8392698551998));
#68197=CARTESIAN_POINT('Ctrl Pts',(-24.7772768358591,27.2887497090376,-59.8451299601413));
#68198=CARTESIAN_POINT('Ctrl Pts',(-24.6664874823241,27.3233048798586,-59.8509900650828));
#68199=CARTESIAN_POINT('Ctrl Pts',(-24.5545016683604,27.3528796066918,-59.8568501700244));
#68200=CARTESIAN_POINT('Ctrl Pts',(-24.4424404389601,27.3824742502526,-59.8627142213798));
#68201=CARTESIAN_POINT('Ctrl Pts',(-24.3291815477118,27.4070816837588,-59.8685782727352));
#68202=CARTESIAN_POINT('Ctrl Pts',(-24.2152066860982,27.4266329274424,-59.8744423240906));
#68203=CARTESIAN_POINT('Ctrl Pts',(-24.1010638482899,27.4462129857564,-59.8803150178872));
#68204=CARTESIAN_POINT('Ctrl Pts',(-23.9862033427299,27.4607219302523,-59.8861877116838));
#68205=CARTESIAN_POINT('Ctrl Pts',(-23.8711108763358,27.4701426988639,-59.8920604054803));
#68206=CARTESIAN_POINT('Ctrl Pts',(-23.8396004842983,27.4727219477196,-59.8936682508037));
#68207=CARTESIAN_POINT('Ctrl Pts',(-23.808072695895,27.4749201021011,-59.8952760961271));
#68208=CARTESIAN_POINT('Ctrl Pts',(-23.7765374399455,27.4767374915912,-59.8968839414504));
#68209=CARTESIAN_POINT('Ctrl Pts',(-23.6613619406432,27.4833751019625,-59.9027562384191));
#68210=CARTESIAN_POINT('Ctrl Pts',(-23.5457011922613,27.4849518748908,-59.9086285353878));
#68211=CARTESIAN_POINT('Ctrl Pts',(-23.4300373447555,27.4814148672928,-59.9145008323565));
#68212=CARTESIAN_POINT('Ctrl Pts',(-23.3145233884103,27.4778824433758,-59.9203655192947));
#68213=CARTESIAN_POINT('Ctrl Pts',(-23.1990067503038,27.4692494302816,-59.9262302062329));
#68214=CARTESIAN_POINT('Ctrl Pts',(-23.0839735020986,27.4555147337185,-59.9320948931711));
#68215=CARTESIAN_POINT('Ctrl Pts',(-22.9690585583877,27.4417941624309,-59.937953548646));
#68216=CARTESIAN_POINT('Ctrl Pts',(-22.8546264237481,27.4229823924681,-59.9438122041208));
#68217=CARTESIAN_POINT('Ctrl Pts',(-22.7411612922178,27.3991303377829,-59.9496708595956));
#68218=CARTESIAN_POINT('Ctrl Pts',(-22.6232641127112,27.3743466008332,-59.9557583593135));
#68219=CARTESIAN_POINT('Ctrl Pts',(-22.5064114748136,27.3441208099937,-59.9618458590314));
#68220=CARTESIAN_POINT('Ctrl Pts',(-22.3911389573759,27.308569272182,-59.9679333587493));
#68221=CARTESIAN_POINT('Ctrl Pts',(-22.2803283080962,27.2743938323168,-59.9737852288327));
#68222=CARTESIAN_POINT('Ctrl Pts',(-22.1709781618021,27.2352974012421,-59.9796370989161));
#68223=CARTESIAN_POINT('Ctrl Pts',(-22.0635512152505,27.1914347841617,-59.9854889689995));
#68224=CARTESIAN_POINT('Ctrl Pts',(-21.9561406254283,27.1475788455636,-59.9913399480825));
#68225=CARTESIAN_POINT('Ctrl Pts',(-21.8506530357254,27.0989583200929,-59.9971909271655));
#68226=CARTESIAN_POINT('Ctrl Pts',(-21.7475321403287,27.0457765540054,-60.0030419062484));
#68227=CARTESIAN_POINT('Ctrl Pts',(-21.6444019733711,26.9925900063655,-60.0088934113907));
#68228=CARTESIAN_POINT('Ctrl Pts',(-21.5436392911471,26.9348415923575,-60.014744916533));
#68229=CARTESIAN_POINT('Ctrl Pts',(-21.4456634727043,26.8727807697653,-60.0205964216753));
#68230=CARTESIAN_POINT('Ctrl Pts',(-21.3476551186254,26.8106993381252,-60.0264498699751));
#68231=CARTESIAN_POINT('Ctrl Pts',(-21.2524358175739,26.7443028714342,-60.0323033182748));
#68232=CARTESIAN_POINT('Ctrl Pts',(-21.1603956359335,26.6738839148418,-60.0381567665746));
#68233=CARTESIAN_POINT('Ctrl Pts',(-21.0682507846201,26.6033848766044,-60.0440168715161));
#68234=CARTESIAN_POINT('Ctrl Pts',(-20.9792925973534,26.5288544693506,-60.0498769764577));
#68235=CARTESIAN_POINT('Ctrl Pts',(-20.8938778035935,26.4506253187524,-60.0557370813992));
#68236=CARTESIAN_POINT('Ctrl Pts',(-20.8084054883159,26.3723434857175,-60.0616011327547));
#68237=CARTESIAN_POINT('Ctrl Pts',(-20.7264816095325,26.2903582412178,-60.0674651841101));
#68238=CARTESIAN_POINT('Ctrl Pts',(-20.6484245757464,26.2050375538908,-60.0733292354656));
#68239=CARTESIAN_POINT('Ctrl Pts',(-20.570252501474,26.1195911209024,-60.0792019292621));
#68240=CARTESIAN_POINT('Ctrl Pts',(-20.4959589104974,26.0307997499948,-60.0850746230587));
#68241=CARTESIAN_POINT('Ctrl Pts',(-20.4258207025986,25.939062851777,-60.0909473168553));
#68242=CARTESIAN_POINT('Ctrl Pts',(-20.4066180345442,25.9139468236151,-60.0925551621787));
#68243=CARTESIAN_POINT('Ctrl Pts',(-20.3877265841919,25.8886101618797,-60.094163007502));
#68244=CARTESIAN_POINT('Ctrl Pts',(-20.369151441206,25.863061398007,-60.0957708528254));
#68245=CARTESIAN_POINT('Ctrl Pts',(-20.3013098682243,25.7697502277949,-60.1016431497941));
#68246=CARTESIAN_POINT('Ctrl Pts',(-20.2374637649966,25.6732952122084,-60.1075154467628));
#68247=CARTESIAN_POINT('Ctrl Pts',(-20.1779182959182,25.574073374114,-60.1133877437315));
#68248=CARTESIAN_POINT('Ctrl Pts',(-20.1184499930387,25.4749801196419,-60.1192524306697));
#68249=CARTESIAN_POINT('Ctrl Pts',(-20.0632714518072,25.3731275242794,-60.1251171176079));
#68250=CARTESIAN_POINT('Ctrl Pts',(-20.0126463352094,25.2689239367605,-60.1309818045461));
#68251=CARTESIAN_POINT('Ctrl Pts',(-19.9620732833747,25.1648275161077,-60.136840460021));
#68252=CARTESIAN_POINT('Ctrl Pts',(-19.9160445211776,25.0583852821121,-60.1426991154958));
#68253=CARTESIAN_POINT('Ctrl Pts',(-19.8747789412593,24.9500321164916,-60.1485577709707));
#68254=CARTESIAN_POINT('Ctrl Pts',(-19.8319014914433,24.8374465807862,-60.1546452706886));
#68255=CARTESIAN_POINT('Ctrl Pts',(-19.7941671518938,24.7227981746295,-60.1607327704065));
#68256=CARTESIAN_POINT('Ctrl Pts',(-19.7617675747234,24.6066003583146,-60.1668202701244));
#68257=CARTESIAN_POINT('Ctrl Pts',(-19.7306220921535,24.4949002258202,-60.1726721402078));
#68258=CARTESIAN_POINT('Ctrl Pts',(-19.7044061858325,24.381768834628,-60.1785240102912));
#68259=CARTESIAN_POINT('Ctrl Pts',(-19.6832397227574,24.267679138058,-60.1843758803746));
#68260=CARTESIAN_POINT('Ctrl Pts',(-19.6620764824688,24.1536068126817,-60.1902268594575));
#68261=CARTESIAN_POINT('Ctrl Pts',(-19.6459612321438,24.0385768783805,-60.1960778385405));
#68262=CARTESIAN_POINT('Ctrl Pts',(-19.634962728683,23.9230725397902,-60.2019288176235));
#68263=CARTESIAN_POINT('Ctrl Pts',(-19.6239632363509,23.8075578162481,-60.2077803227658));
#68264=CARTESIAN_POINT('Ctrl Pts',(-19.6180814445977,23.6915690151714,-60.213631827908));
#68265=CARTESIAN_POINT('Ctrl Pts',(-19.6173341725582,23.5755938096969,-60.2194833330503));
#68266=CARTESIAN_POINT('Ctrl Pts',(-19.6165866523659,23.4595800913813,-60.2253367813501));
#68267=CARTESIAN_POINT('Ctrl Pts',(-19.6209770449584,23.3435803908008,-60.2311902296499));
#68268=CARTESIAN_POINT('Ctrl Pts',(-19.6304700746094,23.2280810104037,-60.2370436779496));
#68269=CARTESIAN_POINT('Ctrl Pts',(-19.6399738998965,23.112450282131,-60.2429037828912));
#68270=CARTESIAN_POINT('Ctrl Pts',(-19.6545919105859,22.9973214219321,-60.2487638878327));
#68271=CARTESIAN_POINT('Ctrl Pts',(-19.6742370905149,22.8831743505639,-60.2546239927742));
#68272=CARTESIAN_POINT('Ctrl Pts',(-19.6938955002431,22.7689504082874,-60.2604880441297));
#68273=CARTESIAN_POINT('Ctrl Pts',(-19.7185877325273,22.6557099742744,-60.2663520954851));
#68274=CARTESIAN_POINT('Ctrl Pts',(-19.7481763224732,22.543919833589,-60.2722161468406));
#68275=CARTESIAN_POINT('Ctrl Pts',(-19.7778085200942,22.4319649365515,-60.2780888406371));
#68276=CARTESIAN_POINT('Ctrl Pts',(-19.8123513547508,22.3214649918376,-60.2839615344337));
#68277=CARTESIAN_POINT('Ctrl Pts',(-19.8516184716668,22.2128688582461,-60.2898342282303));
#68278=CARTESIAN_POINT('Ctrl Pts',(-19.8623691514197,22.1831370534604,-60.2914420735536));
#68279=CARTESIAN_POINT('Ctrl Pts',(-19.8734736802612,22.1535478195493,-60.2930499188769));
#68280=CARTESIAN_POINT('Ctrl Pts',(-19.8849276317304,22.1241100501358,-60.2946577642002));
#68281=CARTESIAN_POINT('Ctrl Pts',(-19.9267606386227,22.0165951532827,-60.300530061169));
#68282=CARTESIAN_POINT('Ctrl Pts',(-19.9733983361586,21.9107423304688,-60.3064023581377));
#68283=CARTESIAN_POINT('Ctrl Pts',(-20.0246884829674,21.8070121184622,-60.3122746551064));
#68284=CARTESIAN_POINT('Ctrl Pts',(-20.0759121618193,21.7034163325723,-60.3181393420446));
#68285=CARTESIAN_POINT('Ctrl Pts',(-20.1317761184858,21.6019380544036,-60.3240040289828));
#68286=CARTESIAN_POINT('Ctrl Pts',(-20.1920793233468,21.5030198378516,-60.329868715921));
#68287=CARTESIAN_POINT('Ctrl Pts',(-20.2523205101368,21.4042033524929,-60.3357273713958));
#68288=CARTESIAN_POINT('Ctrl Pts',(-20.3169916502459,21.3079420426936,-60.3415860268706));
#68289=CARTESIAN_POINT('Ctrl Pts',(-20.3858451911404,21.2146551385099,-60.3474446823455));
#68290=CARTESIAN_POINT('Ctrl Pts',(-20.4573882119876,21.1177243656829,-60.3535321820634));
#68291=CARTESIAN_POINT('Ctrl Pts',(-20.5334468294877,21.0240055088851,-60.3596196817813));
#68292=CARTESIAN_POINT('Ctrl Pts',(-20.613692656973,20.9339373553102,-60.3657071814992));
#68293=CARTESIAN_POINT('Ctrl Pts',(-20.6908323988932,20.8473554813395,-60.3715590515826));
#68294=CARTESIAN_POINT('Ctrl Pts',(-20.771840927712,20.7641472865752,-60.3774109216659));
#68295=CARTESIAN_POINT('Ctrl Pts',(-20.8563851330593,20.6846692684523,-60.3832627917494));
#68296=CARTESIAN_POINT('Ctrl Pts',(-20.9409164657827,20.6052033515803,-60.3891137708323));
#68297=CARTESIAN_POINT('Ctrl Pts',(-21.0289821035365,20.5294667651412,-60.3949647499153));
#68298=CARTESIAN_POINT('Ctrl Pts',(-21.1202126841728,20.4577785480594,-60.4008157289983));
#68299=CARTESIAN_POINT('Ctrl Pts',(-21.2114514673163,20.3860838855169,-60.4066672341406));
#68300=CARTESIAN_POINT('Ctrl Pts',(-21.3058554339614,20.3184385713325,-60.4125187392829));
#68301=CARTESIAN_POINT('Ctrl Pts',(-21.4030233879713,20.2551203637308,-60.4183702444252));
#68302=CARTESIAN_POINT('Ctrl Pts',(-21.5002236093435,20.1917811295308,-60.424223692725));
#68303=CARTESIAN_POINT('Ctrl Pts',(-21.6001892970318,20.1327720847418,-60.4300771410247));
#68304=CARTESIAN_POINT('Ctrl Pts',(-21.7024922486014,20.0783264183927,-60.4359305893245));
#68305=CARTESIAN_POINT('Ctrl Pts',(-21.8049115408417,20.0238188354983,-60.4417906942661));
#68306=CARTESIAN_POINT('Ctrl Pts',(-21.9096730370667,19.9738851835595,-60.4476507992076));
#68307=CARTESIAN_POINT('Ctrl Pts',(-22.0163259359665,19.9287116719331,-60.4535109041491));
#68308=CARTESIAN_POINT('Ctrl Pts',(-22.1230506589182,19.8835077387741,-60.4593749555046));
#68309=CARTESIAN_POINT('Ctrl Pts',(-22.2316689343565,19.8430704729006,-60.46523900686));
#68310=CARTESIAN_POINT('Ctrl Pts',(-22.3417137425724,19.8075365399059,-60.4711030582154));
#68311=CARTESIAN_POINT('Ctrl Pts',(-22.4519207348692,19.771950236987,-60.476975752012));
#68312=CARTESIAN_POINT('Ctrl Pts',(-22.5635580588591,19.7412817988087,-60.4828484458086));
#68313=CARTESIAN_POINT('Ctrl Pts',(-22.6761473494468,19.7156170691804,-60.4887211396052));
#68314=CARTESIAN_POINT('Ctrl Pts',(-22.706972413821,19.7085904955267,-60.4903289849285));
#68315=CARTESIAN_POINT('Ctrl Pts',(-22.7378688013595,19.7019386866499,-60.4919368302518));
#68316=CARTESIAN_POINT('Ctrl Pts',(-22.7688266370183,19.6956627258744,-60.4935446755752));
#68317=CARTESIAN_POINT('Ctrl Pts',(-22.8818932373045,19.6727411768283,-60.4994169725439));
#68318=CARTESIAN_POINT('Ctrl Pts',(-22.9961586457932,19.6547603161135,-60.5052892695126));
#68319=CARTESIAN_POINT('Ctrl Pts',(-23.1111531122592,19.6418410001571,-60.5111615664813));
#68320=CARTESIAN_POINT('Ctrl Pts',(-23.2259985550296,19.6289384266082,-60.5170262534195));
#68321=CARTESIAN_POINT('Ctrl Pts',(-23.3415707699003,19.6210843993312,-60.5228909403577));
#68322=CARTESIAN_POINT('Ctrl Pts',(-23.4573887638217,19.6183490078757,-60.5287556272959));
#68323=CARTESIAN_POINT('Ctrl Pts',(-23.5730876461862,19.615616429599,-60.5346142827707));
#68324=CARTESIAN_POINT('Ctrl Pts',(-23.6890313940491,19.6179920260881,-60.5404729382455));
#68325=CARTESIAN_POINT('Ctrl Pts',(-23.8047334894914,19.6254941388605,-60.5463315937203));
#68326=CARTESIAN_POINT('Ctrl Pts',(-23.9249550106912,19.6332892907655,-60.5524190934382));
#68327=CARTESIAN_POINT('Ctrl Pts',(-24.0449151644658,19.6466196666752,-60.5585065931562));
#68328=CARTESIAN_POINT('Ctrl Pts',(-24.164067284872,19.6654461724555,-60.5645940928741));
#68329=CARTESIAN_POINT('Ctrl Pts',(-24.2786073688293,19.6835439582553,-60.5704459629575));
#68330=CARTESIAN_POINT('Ctrl Pts',(-24.3924003631941,19.7067202360158,-60.5762978330409));
#68331=CARTESIAN_POINT('Ctrl Pts',(-24.5049662804162,19.7348874563703,-60.5821497031243));
#68332=CARTESIAN_POINT('Ctrl Pts',(-24.6175150584538,19.7630503880094,-60.5880006822072));
#68333=CARTESIAN_POINT('Ctrl Pts',(-24.7288367299253,19.7962026509665,-60.5938516612902));
#68334=CARTESIAN_POINT('Ctrl Pts',(-24.8384632261315,19.834205948733,-60.5997026403732));
#68335=CARTESIAN_POINT('Ctrl Pts',(-24.9480995788145,19.8722126633617,-60.6055541455154));
#68336=CARTESIAN_POINT('Ctrl Pts',(-25.0560400626472,19.915071144428,-60.6114056506577));
#68337=CARTESIAN_POINT('Ctrl Pts',(-25.161834131455,19.9625939989862,-60.6172571558));
#68338=CARTESIAN_POINT('Ctrl Pts',(-25.2676633321701,20.0101326348499,-60.6231106040998));
#68339=CARTESIAN_POINT('Ctrl Pts',(-25.3713443236609,20.0623385548715,-60.6289640523995));
#68340=CARTESIAN_POINT('Ctrl Pts',(-25.4724494585164,20.1189775537137,-60.6348175006993));
#68341=CARTESIAN_POINT('Ctrl Pts',(-25.5736695718648,20.1756809633965,-60.6406776056408));
#68342=CARTESIAN_POINT('Ctrl Pts',(-25.6723076209045,20.2368273121739,-60.6465377105823));
#68343=CARTESIAN_POINT('Ctrl Pts',(-25.7679632673607,20.3021379873917,-60.6523978155238));
#68344=CARTESIAN_POINT('Ctrl Pts',(-25.8636833319078,20.3674926452615,-60.6582618668793));
#68345=CARTESIAN_POINT('Ctrl Pts',(-25.9564166646838,20.43701696635,-60.6641259182347));
#68346=CARTESIAN_POINT('Ctrl Pts',(-26.0457958426808,20.5103919126871,-60.6699899695902));
#68347=CARTESIAN_POINT('Ctrl Pts',(-26.1353067477447,20.5838749990484,-60.6758626633867));
#68348=CARTESIAN_POINT('Ctrl Pts',(-26.2214533256054,20.6612197618368,-60.6817353571833));
#68349=CARTESIAN_POINT('Ctrl Pts',(-26.3039047778123,20.7420701466899,-60.6876080509799));
#68350=CARTESIAN_POINT('Ctrl Pts',(-26.3264786061831,20.7642056296018,-60.6892158963033));
#68351=CARTESIAN_POINT('Ctrl Pts',(-26.348775691853,20.7866036941377,-60.6908237416267));
#68352=CARTESIAN_POINT('Ctrl Pts',(-26.3707897855231,20.8092566178404,-60.6924315869501));
#68353=CARTESIAN_POINT('Ctrl Pts',(-26.4501437958303,20.890913413161,-60.6982273728805));
#68354=CARTESIAN_POINT('Ctrl Pts',(-26.52609883446,20.9761737589497,-60.704023158811));
#68355=CARTESIAN_POINT('Ctrl Pts',(-26.5983031636978,21.0647191191764,-60.7098189447415));
#68356=CARTESIAN_POINT('Ctrl Pts',(-26.6703919570342,21.1531227958209,-60.7156054566941));
#68357=CARTESIAN_POINT('Ctrl Pts',(-26.7387417158845,21.2448007023129,-60.7213919686466));
#68358=CARTESIAN_POINT('Ctrl Pts',(-26.8030371795997,21.339397259554,-60.7271784805992));
#68359=CARTESIAN_POINT('Ctrl Pts',(-26.8672738292152,21.4339072848529,-60.7329596993558));
#68360=CARTESIAN_POINT('Ctrl Pts',(-26.9274633142762,21.5313303076372,-60.7387409181124));
#68361=CARTESIAN_POINT('Ctrl Pts',(-26.9833305140211,21.6312776576371,-60.744522136869));
#68362=CARTESIAN_POINT('Ctrl Pts',(-27.0391609827443,21.731159295228,-60.7502995546463));
#68363=CARTESIAN_POINT('Ctrl Pts',(-27.0906746068446,21.8335615920512,-60.7560769724236));
#68364=CARTESIAN_POINT('Ctrl Pts',(-27.1376399857211,21.9380675997803,-60.7618543902008));
#68365=CARTESIAN_POINT('Ctrl Pts',(-27.1845865652934,22.0425317758393,-60.767629495393));
#68366=CARTESIAN_POINT('Ctrl Pts',(-27.2269883454295,22.1490976013021,-60.7734046005852));
#68367=CARTESIAN_POINT('Ctrl Pts',(-27.2646606326085,22.2573250550497,-60.7791797057774));
#68368=CARTESIAN_POINT('Ctrl Pts',(-27.3023402449164,22.3655735529152,-60.7849559339008));
#68369=CARTESIAN_POINT('Ctrl Pts',(-27.3352883768845,22.4754839263879,-60.7907321620243));
#68370=CARTESIAN_POINT('Ctrl Pts',(-27.3633692635136,22.5865981385018,-60.7965083901478));
#68371=CARTESIAN_POINT('Ctrl Pts',(-27.3914519574842,22.6977195021466,-60.8022849900408));
#68372=CARTESIAN_POINT('Ctrl Pts',(-27.4146666867965,22.8100444440291,-60.8080615899338));
#68373=CARTESIAN_POINT('Ctrl Pts',(-27.4329285044896,22.9231031951903,-60.8138381898267));
#68374=CARTESIAN_POINT('Ctrl Pts',(-27.4512067275791,23.0362635120149,-60.8196199790942));
#68375=CARTESIAN_POINT('Ctrl Pts',(-27.4645230919947,23.1501585331982,-60.8254017683616));
#68376=CARTESIAN_POINT('Ctrl Pts',(-27.4728443960287,23.264311863273,-60.8311835576291));
#68377=CARTESIAN_POINT('Ctrl Pts',(-27.4798740195275,23.3607456587816,-60.8360678644078));
#68378=CARTESIAN_POINT('Ctrl Pts',(-27.4833398479381,23.457363568906,-60.8409521711864));
#68379=CARTESIAN_POINT('Ctrl Pts',(-27.4832508599701,23.5538787940674,-60.8458364779651));
#68380=CARTESIAN_POINT('',(-27.4892001437474,23.5489065548291,-62.095836477965));
#68381=CARTESIAN_POINT('Ctrl Pts',(-27.4834099576864,23.553878940757,-60.8458364779651));
#68382=CARTESIAN_POINT('Ctrl Pts',(-27.4861874509236,23.8534728895291,-60.8609971514184));
#68383=CARTESIAN_POINT('Ctrl Pts',(-27.3178909131174,25.4600629410759,-60.9424534619966));
#68384=CARTESIAN_POINT('Ctrl Pts',(-25.1124238142668,27.9320754076231,-61.0902054096999));
#68385=CARTESIAN_POINT('Ctrl Pts',(-20.7081712302401,27.2330944653146,-61.2890923210748));
#68386=CARTESIAN_POINT('Ctrl Pts',(-18.9155503934932,23.1498940395121,-61.4879792324495));
#68387=CARTESIAN_POINT('Ctrl Pts',(-21.3818278638133,19.4345891232223,-61.6868661438245));
#68388=CARTESIAN_POINT('Ctrl Pts',(-25.8407037518232,19.5012299286061,-61.8857530551994));
#68389=CARTESIAN_POINT('Ctrl Pts',(-27.4543102486202,22.0972001521906,-62.0220764999129));
#68390=CARTESIAN_POINT('Ctrl Pts',(-27.4895254076886,23.4754357787105,-62.0921043075015));
#68391=CARTESIAN_POINT('Ctrl Pts',(-27.4892001437474,23.5489065548291,-62.095836477965));
#68392=CARTESIAN_POINT('',(-27.4820679227229,23.5472708336066,-63.3458360315144));
#68393=CARTESIAN_POINT('Ctrl Pts',(-27.4892001437474,23.5489065548291,-62.095836477965));
#68394=CARTESIAN_POINT('Ctrl Pts',(-27.4837476490292,24.7805186950384,-62.1583999446264));
#68395=CARTESIAN_POINT('Ctrl Pts',(-26.1980019261252,27.3270249273693,-62.2872590484128));
#68396=CARTESIAN_POINT('Ctrl Pts',(-21.8578298400895,27.8834333801068,-62.4824137893241));
#68397=CARTESIAN_POINT('Ctrl Pts',(-18.9898485690431,24.4686568705032,-62.681300700699));
#68398=CARTESIAN_POINT('Ctrl Pts',(-20.3124918811797,20.209944641381,-62.8801876120739));
#68399=CARTESIAN_POINT('Ctrl Pts',(-24.6103627143063,19.0206921520514,-63.0790745234488));
#68400=CARTESIAN_POINT('Ctrl Pts',(-27.2042676807139,21.3409108015181,-63.2342903151889));
#68401=CARTESIAN_POINT('Ctrl Pts',(-27.4824290166878,23.0989765952615,-63.3232104698041));
#68402=CARTESIAN_POINT('Ctrl Pts',(-27.4792998261461,23.5472522368032,-63.3458349872944));
#68403=CARTESIAN_POINT('',(-27.4816133133806,23.5527675431246,-64.5958369912555));
#68404=CARTESIAN_POINT('Ctrl Pts',(-27.4832514074667,23.5472787845695,-63.3458364779651));
#68405=CARTESIAN_POINT('Ctrl Pts',(-27.48333921894,23.6634159041666,-63.3516920745539));
#68406=CARTESIAN_POINT('Ctrl Pts',(-27.4782786202806,23.7796066600921,-63.3575476711427));
#68407=CARTESIAN_POINT('Ctrl Pts',(-27.4680820905473,23.8953620038579,-63.3634032677314));
#68408=CARTESIAN_POINT('Ctrl Pts',(-27.4578867609682,24.011103722962,-63.3692581751035));
#68409=CARTESIAN_POINT('Ctrl Pts',(-27.4425567381748,24.1264097214561,-63.3751130824755));
#68410=CARTESIAN_POINT('Ctrl Pts',(-27.4221564839496,24.2407949159899,-63.3809679898475));
#68411=CARTESIAN_POINT('Ctrl Pts',(-27.401753732463,24.3551941127874,-63.3868236139378));
#68412=CARTESIAN_POINT('Ctrl Pts',(-27.3762795874776,24.4686718758199,-63.3926792380281));
#68413=CARTESIAN_POINT('Ctrl Pts',(-27.3458497277285,24.5807528594265,-63.3985348621183));
#68414=CARTESIAN_POINT('Ctrl Pts',(-27.3154088362872,24.6928744755873,-63.4043926090394));
#68415=CARTESIAN_POINT('Ctrl Pts',(-27.2800087648194,24.8035979078446,-63.4102503559605));
#68416=CARTESIAN_POINT('Ctrl Pts',(-27.239814986766,24.9124631945965,-63.4161081028815));
#68417=CARTESIAN_POINT('Ctrl Pts',(-27.1995721439576,25.0214613737729,-63.4219730003849));
#68418=CARTESIAN_POINT('Ctrl Pts',(-27.1545240553449,25.128596492421,-63.4278378978882));
#68419=CARTESIAN_POINT('Ctrl Pts',(-27.1048843389936,25.2334286111748,-63.4337027953915));
#68420=CARTESIAN_POINT('Ctrl Pts',(-27.0552101520406,25.3383335270047,-63.4395717655722));
#68421=CARTESIAN_POINT('Ctrl Pts',(-27.0009381802215,25.4409318949764,-63.4454407357528));
#68422=CARTESIAN_POINT('Ctrl Pts',(-26.9423270985381,25.5408100247023,-63.4513097059334));
#68423=CARTESIAN_POINT('Ctrl Pts',(-26.8836219472568,25.6408484568017,-63.4571880956922));
#68424=CARTESIAN_POINT('Ctrl Pts',(-26.8205640056903,25.738157589445,-63.4630664854511));
#68425=CARTESIAN_POINT('Ctrl Pts',(-26.7534543272939,25.8323540317741,-63.4689448752099));
#68426=CARTESIAN_POINT('Ctrl Pts',(-26.7233780979169,25.874569608926,-63.4715793655394));
#68427=CARTESIAN_POINT('Ctrl Pts',(-26.6924885943787,25.9161604565012,-63.4742138558689));
#68428=CARTESIAN_POINT('Ctrl Pts',(-26.660815366584,25.9570944147855,-63.4768483461985));
#68429=CARTESIAN_POINT('Ctrl Pts',(-26.5902155251335,26.0483364878555,-63.4827206431672));
#68430=CARTESIAN_POINT('Ctrl Pts',(-26.5154794034389,26.1366224269578,-63.4885929401359));
#68431=CARTESIAN_POINT('Ctrl Pts',(-26.4368835706086,26.2215537586576,-63.4944652371046));
#68432=CARTESIAN_POINT('Ctrl Pts',(-26.3583895917357,26.3063750260966,-63.5003299240428));
#68433=CARTESIAN_POINT('Ctrl Pts',(-26.276046126848,26.3878500307594,-63.506194610981));
#68434=CARTESIAN_POINT('Ctrl Pts',(-26.1901714325743,26.4656113769782,-63.5120592979192));
#68435=CARTESIAN_POINT('Ctrl Pts',(-26.1043850550479,26.5432927505205,-63.517917953394));
#68436=CARTESIAN_POINT('Ctrl Pts',(-26.0150749762511,26.6172677865298,-63.5237766088688));
#68437=CARTESIAN_POINT('Ctrl Pts',(-25.9225974536442,26.6872046466137,-63.5296352643436));
#68438=CARTESIAN_POINT('Ctrl Pts',(-25.8265076775513,26.7598733020519,-63.5357227640615));
#68439=CARTESIAN_POINT('Ctrl Pts',(-25.7269982757149,26.8281815472473,-63.5418102637794));
#68440=CARTESIAN_POINT('Ctrl Pts',(-25.624508567612,26.8918017079684,-63.5478977634973));
#68441=CARTESIAN_POINT('Ctrl Pts',(-25.525985941822,26.9529593149461,-63.5537496335807));
#68442=CARTESIAN_POINT('Ctrl Pts',(-25.4247098219172,27.0097847753873,-63.5596015036641));
#68443=CARTESIAN_POINT('Ctrl Pts',(-25.3211007257736,27.0620306672725,-63.5654533737475));
#68444=CARTESIAN_POINT('Ctrl Pts',(-25.2175074050572,27.1142686042455,-63.5713043528305));
#68445=CARTESIAN_POINT('Ctrl Pts',(-25.1115821833953,27.161928173004,-63.5771553319135));
#68446=CARTESIAN_POINT('Ctrl Pts',(-25.0037697222696,27.2048081512876,-63.5830063109964));
#68447=CARTESIAN_POINT('Ctrl Pts',(-24.895947567766,27.247691984894,-63.5888578161387));
#68448=CARTESIAN_POINT('Ctrl Pts',(-24.786238220628,27.2857952209766,-63.594709321281));
#68449=CARTESIAN_POINT('Ctrl Pts',(-24.6751051657447,27.3189652498076,-63.6005608264233));
#68450=CARTESIAN_POINT('Ctrl Pts',(-24.5639352059935,27.352146293683,-63.6064142747231));
#68451=CARTESIAN_POINT('Ctrl Pts',(-24.4513409943046,27.3803907546614,-63.6122677230228));
#68452=CARTESIAN_POINT('Ctrl Pts',(-24.3377992770121,27.4035964203108,-63.6181211713226));
#68453=CARTESIAN_POINT('Ctrl Pts',(-24.2241284381315,27.4268284758412,-63.6239812762641));
#68454=CARTESIAN_POINT('Ctrl Pts',(-24.1095083482015,27.4450102159024,-63.6298413812057));
#68455=CARTESIAN_POINT('Ctrl Pts',(-23.9944241050035,27.4580908872898,-63.6357014861472));
#68456=CARTESIAN_POINT('Ctrl Pts',(-23.8792623597704,27.4711803676906,-63.6415655375027));
#68457=CARTESIAN_POINT('Ctrl Pts',(-23.7636362502579,27.4791619107537,-63.6474295888582));
#68458=CARTESIAN_POINT('Ctrl Pts',(-23.6480323800569,27.4820368723281,-63.6532936402136));
#68459=CARTESIAN_POINT('Ctrl Pts',(-23.5322581328281,27.484916071022,-63.6591663340102));
#68460=CARTESIAN_POINT('Ctrl Pts',(-23.4165066020795,27.4826736755969,-63.6650390278068));
#68461=CARTESIAN_POINT('Ctrl Pts',(-23.301260861813,27.4753629948952,-63.6709117216034));
#68462=CARTESIAN_POINT('Ctrl Pts',(-23.2697085059534,27.4733614528118,-63.6725195669267));
#68463=CARTESIAN_POINT('Ctrl Pts',(-23.2381940101071,27.4709803027052,-63.6741274122501));
#68464=CARTESIAN_POINT('Ctrl Pts',(-23.206727151238,27.4682213055594,-63.6757352575734));
#68465=CARTESIAN_POINT('Ctrl Pts',(-23.0918014570385,27.4581446829259,-63.6816075545421));
#68466=CARTESIAN_POINT('Ctrl Pts',(-22.9771269731236,27.4429902225945,-63.6874798515108));
#68467=CARTESIAN_POINT('Ctrl Pts',(-22.8631884392071,27.4227752150125,-63.6933521484795));
#68468=CARTESIAN_POINT('Ctrl Pts',(-22.7493975605817,27.4025864044749,-63.6992168354177));
#68469=CARTESIAN_POINT('Ctrl Pts',(-22.636341138592,27.3773501598767,-63.7050815223559));
#68470=CARTESIAN_POINT('Ctrl Pts',(-22.5245003005774,27.3471356429262,-63.7109462092941));
#68471=CARTESIAN_POINT('Ctrl Pts',(-22.4127744838634,27.3169521997149,-63.716804864769));
#68472=CARTESIAN_POINT('Ctrl Pts',(-22.3022621611847,27.2818007749441,-63.7226635202438));
#68473=CARTESIAN_POINT('Ctrl Pts',(-22.1934350860089,27.2418017212736,-63.7285221757186));
#68474=CARTESIAN_POINT('Ctrl Pts',(-22.0803571294231,27.2002402693359,-63.7346096754365));
#68475=CARTESIAN_POINT('Ctrl Pts',(-21.969099206452,27.1534448422978,-63.7406971751544));
#68476=CARTESIAN_POINT('Ctrl Pts',(-21.8601744657258,27.1016079251929,-63.7467846748723));
#68477=CARTESIAN_POINT('Ctrl Pts',(-21.755465888948,27.0517774663053,-63.7526365449557));
#68478=CARTESIAN_POINT('Ctrl Pts',(-21.6529136394392,26.9972887377645,-63.7584884150391));
#68479=CARTESIAN_POINT('Ctrl Pts',(-21.5529531852349,26.9383617862244,-63.7643402851225));
#68480=CARTESIAN_POINT('Ctrl Pts',(-21.4530079509187,26.8794438068486,-63.7701912642055));
#68481=CARTESIAN_POINT('Ctrl Pts',(-21.3556540832809,26.8160891579714,-63.7760422432885));
#68482=CARTESIAN_POINT('Ctrl Pts',(-21.2613012323669,26.7485631715958,-63.7818932223714));
#68483=CARTESIAN_POINT('Ctrl Pts',(-21.1669398982235,26.6810311139842,-63.7877447275137));
#68484=CARTESIAN_POINT('Ctrl Pts',(-21.0755804533642,26.6093272139199,-63.793596232656));
#68485=CARTESIAN_POINT('Ctrl Pts',(-20.9876018241446,26.5337589169891,-63.7994477377983));
#68486=CARTESIAN_POINT('Ctrl Pts',(-20.8995939791375,26.458165525472,-63.8053011860981));
#68487=CARTESIAN_POINT('Ctrl Pts',(-20.8149694955982,26.3787054545708,-63.8111546343979));
#68488=CARTESIAN_POINT('Ctrl Pts',(-20.734072068165,26.2957245488229,-63.8170080826977));
#68489=CARTESIAN_POINT('Ctrl Pts',(-20.6530826427903,26.2126492757661,-63.8228681876392));
#68490=CARTESIAN_POINT('Ctrl Pts',(-20.5758290221214,26.1260454722655,-63.8287282925807));
#68491=CARTESIAN_POINT('Ctrl Pts',(-20.5026161215967,26.036293824965,-63.8345883975223));
#68492=CARTESIAN_POINT('Ctrl Pts',(-20.4293539167658,25.9464817355477,-63.8404524488777));
#68493=CARTESIAN_POINT('Ctrl Pts',(-20.3601380967407,25.853517911999,-63.8463165002331));
#68494=CARTESIAN_POINT('Ctrl Pts',(-20.2952305506919,25.7578124749782,-63.8521805515886));
#68495=CARTESIAN_POINT('Ctrl Pts',(-20.230227343877,25.6619659872478,-63.8580532453851));
#68496=CARTESIAN_POINT('Ctrl Pts',(-20.1695452993464,25.5633701725322,-63.8639259391817));
#68497=CARTESIAN_POINT('Ctrl Pts',(-20.1134006894535,25.4624602647835,-63.8697986329783));
#68498=CARTESIAN_POINT('Ctrl Pts',(-20.0980292344491,25.434832820058,-63.8714064783016));
#68499=CARTESIAN_POINT('Ctrl Pts',(-20.0829976149859,25.4070320333676,-63.873014323625));
#68500=CARTESIAN_POINT('Ctrl Pts',(-20.0683096343822,25.3790670821226,-63.8746221689483));
#68501=CARTESIAN_POINT('Ctrl Pts',(-20.014665056311,25.2769313256291,-63.880494465917));
#68502=CARTESIAN_POINT('Ctrl Pts',(-19.9654283381006,25.1722621300223,-63.8863667628857));
#68503=CARTESIAN_POINT('Ctrl Pts',(-19.9208469553725,25.0654766611764,-63.8922390598544));
#68504=CARTESIAN_POINT('Ctrl Pts',(-19.8763233465758,24.9588295778171,-63.8981037467927));
#68505=CARTESIAN_POINT('Ctrl Pts',(-19.8364432336887,24.8500720530627,-63.9039684337309));
#68506=CARTESIAN_POINT('Ctrl Pts',(-19.8014084995292,24.7396462522514,-63.9098331206691));
#68507=CARTESIAN_POINT('Ctrl Pts',(-19.7664097964007,24.6293340174638,-63.9156917761439));
#68508=CARTESIAN_POINT('Ctrl Pts',(-19.7362466844819,24.5173573109278,-63.9215504316187));
#68509=CARTESIAN_POINT('Ctrl Pts',(-19.7110729118093,24.4041780824656,-63.9274090870936));
#68510=CARTESIAN_POINT('Ctrl Pts',(-19.6849158294033,24.2865779736527,-63.9334965868115));
#68511=CARTESIAN_POINT('Ctrl Pts',(-19.6641459833917,24.1676799042311,-63.9395840865293));
#68512=CARTESIAN_POINT('Ctrl Pts',(-19.6488788114747,24.048019641074,-63.9456715862472));
#68513=CARTESIAN_POINT('Ctrl Pts',(-19.6342025879445,23.9329910831126,-63.9515234563306));
#68514=CARTESIAN_POINT('Ctrl Pts',(-19.6246110311334,23.8172586872364,-63.9573753264141));
#68515=CARTESIAN_POINT('Ctrl Pts',(-19.6201544010332,23.7013077645549,-63.9632271964974));
#68516=CARTESIAN_POINT('Ctrl Pts',(-19.6156984494954,23.5853744964557,-63.9690781755804));
#68517=CARTESIAN_POINT('Ctrl Pts',(-19.6163758859941,23.4692231806724,-63.9749291546634));
#68518=CARTESIAN_POINT('Ctrl Pts',(-19.6221849154793,23.3533418858573,-63.9807801337463));
#68519=CARTESIAN_POINT('Ctrl Pts',(-19.6279944672522,23.2374501721985,-63.9866316388886));
#68520=CARTESIAN_POINT('Ctrl Pts',(-19.6389365084938,23.1218289406583,-63.9924831440309));
#68521=CARTESIAN_POINT('Ctrl Pts',(-19.6549572058332,23.0069631757101,-63.9983346491732));
#68522=CARTESIAN_POINT('Ctrl Pts',(-19.6709832232975,22.892059266342,-64.004188097473));
#68523=CARTESIAN_POINT('Ctrl Pts',(-19.6920911933078,22.7779117316164,-64.0100415457727));
#68524=CARTESIAN_POINT('Ctrl Pts',(-19.7181759325748,22.6649966712328,-64.0158949940725));
#68525=CARTESIAN_POINT('Ctrl Pts',(-19.7442903358544,22.5519532019065,-64.021755099014));
#68526=CARTESIAN_POINT('Ctrl Pts',(-19.7753927118145,22.4401454074695,-64.0276152039556));
#68527=CARTESIAN_POINT('Ctrl Pts',(-19.811327602115,22.3300355956655,-64.0334753088971));
#68528=CARTESIAN_POINT('Ctrl Pts',(-19.847286692315,22.2198516317948,-64.0393393602526));
#68529=CARTESIAN_POINT('Ctrl Pts',(-19.8880846318463,22.1113683134429,-64.045203411608));
#68530=CARTESIAN_POINT('Ctrl Pts',(-19.933517941516,22.0050276599657,-64.0510674629635));
#68531=CARTESIAN_POINT('Ctrl Pts',(-19.9790182108148,21.898530281593,-64.0569401567601));
#68532=CARTESIAN_POINT('Ctrl Pts',(-20.0291673064368,21.7941822417638,-64.0628128505566));
#68533=CARTESIAN_POINT('Ctrl Pts',(-20.0837159631312,21.6924007564398,-64.0686855443532));
#68534=CARTESIAN_POINT('Ctrl Pts',(-20.0986504728465,21.6645346883547,-64.0702933896765));
#68535=CARTESIAN_POINT('Ctrl Pts',(-20.1139145135817,21.6368608309317,-64.0719012349999));
#68536=CARTESIAN_POINT('Ctrl Pts',(-20.1295024200826,21.6093873447456,-64.0735090803232));
#68537=CARTESIAN_POINT('Ctrl Pts',(-20.186433777077,21.5090465549255,-64.0793813772919));
#68538=CARTESIAN_POINT('Ctrl Pts',(-20.2478791940212,21.4110447403216,-64.0852536742606));
#68539=CARTESIAN_POINT('Ctrl Pts',(-20.3136214733308,21.3158156021665,-64.0911259712293));
#68540=CARTESIAN_POINT('Ctrl Pts',(-20.3792785558675,21.2207098734114,-64.0969906581675));
#68541=CARTESIAN_POINT('Ctrl Pts',(-20.4492211945505,21.1283700126328,-64.1028553451057));
#68542=CARTESIAN_POINT('Ctrl Pts',(-20.5231865144831,21.0392048763428,-64.1087200320439));
#68543=CARTESIAN_POINT('Ctrl Pts',(-20.5970757657147,20.9501314408134,-64.1145786875187));
#68544=CARTESIAN_POINT('Ctrl Pts',(-20.6749792069993,20.8642265517596,-64.1204373429936));
#68545=CARTESIAN_POINT('Ctrl Pts',(-20.7565912995322,20.7818692634463,-64.1262959984684));
#68546=CARTESIAN_POINT('Ctrl Pts',(-20.8413912322822,20.6962950269123,-64.1323834981863));
#68547=CARTESIAN_POINT('Ctrl Pts',(-20.9301951907223,20.6145515600119,-64.1384709979042));
#68548=CARTESIAN_POINT('Ctrl Pts',(-21.0226148241633,20.5370255871266,-64.1445584976221));
#68549=CARTESIAN_POINT('Ctrl Pts',(-21.1114571589664,20.4625004220446,-64.1504103677055));
#68550=CARTESIAN_POINT('Ctrl Pts',(-21.2036401223324,20.3918726181543,-64.1562622377889));
#68551=CARTESIAN_POINT('Ctrl Pts',(-21.2987825815385,20.3254467912587,-64.1621141078723));
#68552=CARTESIAN_POINT('Ctrl Pts',(-21.39391055444,20.2590310782992,-64.1679650869553));
#68553=CARTESIAN_POINT('Ctrl Pts',(-21.49199678837,20.1968163068072,-64.1738160660383));
#68554=CARTESIAN_POINT('Ctrl Pts',(-21.592629692682,20.139064788374,-64.1796670451212));
#68555=CARTESIAN_POINT('Ctrl Pts',(-21.6932716448603,20.0813080775237,-64.1855185502635));
#68556=CARTESIAN_POINT('Ctrl Pts',(-21.7964603640337,20.0280156232292,-64.1913700554058));
#68557=CARTESIAN_POINT('Ctrl Pts',(-21.901758725408,19.9794042892403,-64.1972215605481));
#68558=CARTESIAN_POINT('Ctrl Pts',(-22.0070920540762,19.9307768124854,-64.2030750088479));
#68559=CARTESIAN_POINT('Ctrl Pts',(-22.1145360428575,19.8868337202332,-64.2089284571477));
#68560=CARTESIAN_POINT('Ctrl Pts',(-22.2236332850595,19.8477438720881,-64.2147819054474));
#68561=CARTESIAN_POINT('Ctrl Pts',(-22.3328545945158,19.8086095702975,-64.220642010389));
#68562=CARTESIAN_POINT('Ctrl Pts',(-22.4437325206441,19.774339668274,-64.2265021153305));
#68563=CARTESIAN_POINT('Ctrl Pts',(-22.5557940843599,19.745053273242,-64.2323622202721));
#68564=CARTESIAN_POINT('Ctrl Pts',(-22.667931114525,19.7157471556559,-64.2382262716275));
#68565=CARTESIAN_POINT('Ctrl Pts',(-22.7812529662782,19.6914313141979,-64.244090322983));
#68566=CARTESIAN_POINT('Ctrl Pts',(-22.8952777721892,19.6721734886097,-64.2499543743384));
#68567=CARTESIAN_POINT('Ctrl Pts',(-23.0094706279027,19.6528872808307,-64.255827068135));
#68568=CARTESIAN_POINT('Ctrl Pts',(-23.1243680967429,19.6386740172364,-64.2616997619315));
#68569=CARTESIAN_POINT('Ctrl Pts',(-23.2394844294858,19.6295495097031,-64.2675724557281));
#68570=CARTESIAN_POINT('Ctrl Pts',(-23.27100135573,19.6270513721749,-64.2691803010514));
#68571=CARTESIAN_POINT('Ctrl Pts',(-23.3025346974053,19.624934372634,-64.2707881463748));
#68572=CARTESIAN_POINT('Ctrl Pts',(-23.3340745265731,19.6231981559436,-64.2723959916981));
#68573=CARTESIAN_POINT('Ctrl Pts',(-23.4492667285384,19.6168570111456,-64.2782682886669));
#68574=CARTESIAN_POINT('Ctrl Pts',(-23.564931152178,19.615577935982,-64.2841405856356));
#68575=CARTESIAN_POINT('Ctrl Pts',(-23.6805855128659,19.6194126323827,-64.2900128826043));
#68576=CARTESIAN_POINT('Ctrl Pts',(-23.796089994687,19.6232423593215,-64.2958775695425));
#68577=CARTESIAN_POINT('Ctrl Pts',(-23.9115840301476,19.632172665445,-64.3017422564807));
#68578=CARTESIAN_POINT('Ctrl Pts',(-24.0265815463789,19.6462033939694,-64.3076069434188));
#68579=CARTESIAN_POINT('Ctrl Pts',(-24.141460794864,19.660219692768,-64.3134655988937));
#68580=CARTESIAN_POINT('Ctrl Pts',(-24.2558441319339,19.6793259307035,-64.3193242543685));
#68581=CARTESIAN_POINT('Ctrl Pts',(-24.3692474961989,19.7034699477527,-64.3251829098433));
#68582=CARTESIAN_POINT('Ctrl Pts',(-24.4870804957564,19.7285570513735,-64.3312704095612));
#68583=CARTESIAN_POINT('Ctrl Pts',(-24.6038549501757,19.7590835023726,-64.3373579092791));
#68584=CARTESIAN_POINT('Ctrl Pts',(-24.7190355817353,19.7949316157222,-64.343445408997));
#68585=CARTESIAN_POINT('Ctrl Pts',(-24.8297579017756,19.8293921515379,-64.3492972790804));
#68586=CARTESIAN_POINT('Ctrl Pts',(-24.9390070578119,19.8687699031585,-64.3551491491638));
#68587=CARTESIAN_POINT('Ctrl Pts',(-25.0463207530643,19.9129088749844,-64.3610010192472));
#68588=CARTESIAN_POINT('Ctrl Pts',(-25.1536181088305,19.9570411262505,-64.3668519983302));
#68589=CARTESIAN_POINT('Ctrl Pts',(-25.2589802075513,20.0059329991081,-64.3727029774131));
#68590=CARTESIAN_POINT('Ctrl Pts',(-25.3619638798905,20.0593800059756,-64.3785539564961));
#68591=CARTESIAN_POINT('Ctrl Pts',(-25.4649568114528,20.1128318182434,-64.3844054616384));
#68592=CARTESIAN_POINT('Ctrl Pts',(-25.5655705245983,20.1708393882361,-64.3902569667807));
#68593=CARTESIAN_POINT('Ctrl Pts',(-25.6633862837334,20.2331521795805,-64.396108471923));
#68594=CARTESIAN_POINT('Ctrl Pts',(-25.7612345253536,20.295485663647,-64.4019619202228));
#68595=CARTESIAN_POINT('Ctrl Pts',(-25.8562826169643,20.3621269898886,-64.4078153685225));
#68596=CARTESIAN_POINT('Ctrl Pts',(-25.9481412464389,20.4327826101553,-64.4136688168223));
#68597=CARTESIAN_POINT('Ctrl Pts',(-26.0401043391214,20.5035185812043,-64.4195289217639));
#68598=CARTESIAN_POINT('Ctrl Pts',(-26.1288704022038,20.5782777059454,-64.4253890267054));
#68599=CARTESIAN_POINT('Ctrl Pts',(-26.2140835635339,20.6567264416428,-64.431249131647));
#68600=CARTESIAN_POINT('Ctrl Pts',(-26.2993541105949,20.7352280076539,-64.4371131830024));
#68601=CARTESIAN_POINT('Ctrl Pts',(-26.3810667009177,20.8174238397464,-64.4429772343579));
#68602=CARTESIAN_POINT('Ctrl Pts',(-26.4589038741473,20.9029451509683,-64.4488412857133));
#68603=CARTESIAN_POINT('Ctrl Pts',(-26.5368557638323,20.9885925035311,-64.4547139795099));
#68604=CARTESIAN_POINT('Ctrl Pts',(-26.6109205737252,21.0775748003285,-64.4605866733064));
#68605=CARTESIAN_POINT('Ctrl Pts',(-26.6808224329813,21.1694919193782,-64.466459367103));
#68606=CARTESIAN_POINT('Ctrl Pts',(-26.6999603927303,21.1946572889883,-64.4680672124263));
#68607=CARTESIAN_POINT('Ctrl Pts',(-26.718786567932,21.2200424904158,-64.4696750577496));
#68608=CARTESIAN_POINT('Ctrl Pts',(-26.7372958908976,21.2456389791528,-64.471282903073));
#68609=CARTESIAN_POINT('Ctrl Pts',(-26.8054318389887,21.339863983014,-64.4772016536233));
#68610=CARTESIAN_POINT('Ctrl Pts',(-26.8694982636535,21.4372688892917,-64.4831204041736));
#68611=CARTESIAN_POINT('Ctrl Pts',(-26.9291869163797,21.5374705206483,-64.4890391547239));
#68612=CARTESIAN_POINT('Ctrl Pts',(-26.988795941757,21.6375384785194,-64.4949500093947));
#68613=CARTESIAN_POINT('Ctrl Pts',(-27.0440386046206,21.7403953974653,-64.5008608640654));
#68614=CARTESIAN_POINT('Ctrl Pts',(-27.0946481205995,21.8456267929032,-64.5067717187361));
#68615=CARTESIAN_POINT('Ctrl Pts',(-27.1452017244463,21.9507419313177,-64.5126760432419));
#68616=CARTESIAN_POINT('Ctrl Pts',(-27.1911321889275,22.0582259658421,-64.5185803677477));
#68617=CARTESIAN_POINT('Ctrl Pts',(-27.2322174367539,22.1676378211156,-64.5244846922535));
#68618=CARTESIAN_POINT('Ctrl Pts',(-27.273592559287,22.2778216257168,-64.5304306743961));
#68619=CARTESIAN_POINT('Ctrl Pts',(-27.3100536038442,22.3899602092726,-64.5363766565388));
#68620=CARTESIAN_POINT('Ctrl Pts',(-27.3414218951241,22.5035797758673,-64.5423226386814));
#68621=CARTESIAN_POINT('Ctrl Pts',(-27.3725217740672,22.6162271220402,-64.5482177422171));
#68622=CARTESIAN_POINT('Ctrl Pts',(-27.3986156100069,22.7303298065523,-64.5541128457528));
#68623=CARTESIAN_POINT('Ctrl Pts',(-27.4195786389942,22.8454089494954,-64.5600079492885));
#68624=CARTESIAN_POINT('Ctrl Pts',(-27.4408130549991,22.9619779050709,-64.5659793707346));
#68625=CARTESIAN_POINT('Ctrl Pts',(-27.456782747268,23.0795483776637,-64.5719507921807));
#68626=CARTESIAN_POINT('Ctrl Pts',(-27.4674113082267,23.1976109013743,-64.5779222136267));
#68627=CARTESIAN_POINT('Ctrl Pts',(-27.4780398691853,23.315673425085,-64.5838936350728));
#68628=CARTESIAN_POINT('Ctrl Pts',(-27.4833272543798,23.4342275698376,-64.5898650565189));
#68629=CARTESIAN_POINT('Ctrl Pts',(-27.4832517333937,23.5527584109668,-64.595836477965));
#68630=CARTESIAN_POINT('',(-27.4850627174193,23.5522765954312,-65.8458358713706));
#68631=CARTESIAN_POINT('Ctrl Pts',(-27.478390383421,23.5527855069586,-64.5958380009472));
#68632=CARTESIAN_POINT('Ctrl Pts',(-27.4812350713865,24.0440006034334,-64.6206152721141));
#68633=CARTESIAN_POINT('Ctrl Pts',(-27.1676348699015,25.8460339334477,-64.7116881804063));
#68634=CARTESIAN_POINT('Ctrl Pts',(-24.4627872245136,28.1118346329514,-64.8690567258226));
#68635=CARTESIAN_POINT('Ctrl Pts',(-20.2057806611153,26.7837117844163,-65.0679436371978));
#68636=CARTESIAN_POINT('Ctrl Pts',(-19.0220601823267,22.4843140347648,-65.2668305485724));
#68637=CARTESIAN_POINT('Ctrl Pts',(-21.999364545208,19.1644233871103,-65.4657174599474));
#68638=CARTESIAN_POINT('Ctrl Pts',(-26.2715252890564,19.8537180446844,-65.6587188550772));
#68639=CARTESIAN_POINT('Ctrl Pts',(-27.4809586739053,22.3624402719865,-65.7854246130821));
#68640=CARTESIAN_POINT('Ctrl Pts',(-27.4884579349096,23.5522559503263,-65.845834733962));
#68641=CARTESIAN_POINT('',(-27.4832509814148,23.5467604699193,-67.0958364779651));
#68642=CARTESIAN_POINT('Ctrl Pts',(-27.4832520051843,23.5522876057256,-65.845836477965));
#68643=CARTESIAN_POINT('Ctrl Pts',(-27.4831921100013,23.6680414897683,-65.8517214128757));
#68644=CARTESIAN_POINT('Ctrl Pts',(-27.4780224898854,23.7836598109612,-65.8576063477865));
#68645=CARTESIAN_POINT('Ctrl Pts',(-27.4677759706825,23.8988197489962,-65.8634912826973));
#68646=CARTESIAN_POINT('Ctrl Pts',(-27.4575514559566,24.0137323801976,-65.8693635796661));
#68647=CARTESIAN_POINT('Ctrl Pts',(-27.4422494310259,24.1283872665401,-65.8752358766348));
#68648=CARTESIAN_POINT('Ctrl Pts',(-27.4218878101455,24.2422996909625,-65.8811081736036));
#68649=CARTESIAN_POINT('Ctrl Pts',(-27.4015525763087,24.3560644939294,-65.8869728605419));
#68650=CARTESIAN_POINT('Ctrl Pts',(-27.3761708577797,24.4690883452134,-65.8928375474801));
#68651=CARTESIAN_POINT('Ctrl Pts',(-27.3458124353828,24.5808902068794,-65.8987022344183));
#68652=CARTESIAN_POINT('Ctrl Pts',(-27.3154852347229,24.6925770873298,-65.9045608898932));
#68653=CARTESIAN_POINT('Ctrl Pts',(-27.2801916182897,24.8030440813435,-65.910419545368));
#68654=CARTESIAN_POINT('Ctrl Pts',(-27.2400525457537,24.9118195907283,-65.9162782008429));
#68655=CARTESIAN_POINT('Ctrl Pts',(-27.1983456056905,25.0248439673173,-65.9223657005608));
#68656=CARTESIAN_POINT('Ctrl Pts',(-27.1514070371028,25.1360415760795,-65.9284532002787));
#68657=CARTESIAN_POINT('Ctrl Pts',(-27.0994299852475,25.244899516523,-65.9345406999966));
#68658=CARTESIAN_POINT('Ctrl Pts',(-27.049464815823,25.3495438786655,-65.94039257008));
#68659=CARTESIAN_POINT('Ctrl Pts',(-26.9948441556283,25.4520259204937,-65.9462444401634));
#68660=CARTESIAN_POINT('Ctrl Pts',(-26.9357886115487,25.5519104575155,-65.9520963102468));
#68661=CARTESIAN_POINT('Ctrl Pts',(-26.8767420592127,25.6517797862084,-65.9579472893297));
#68662=CARTESIAN_POINT('Ctrl Pts',(-26.8132621759368,25.7490520407199,-65.9637982684127));
#68663=CARTESIAN_POINT('Ctrl Pts',(-26.745614820692,25.8433179128055,-65.9696492474957));
#68664=CARTESIAN_POINT('Ctrl Pts',(-26.6779613832989,25.9375922603001,-65.9755007526379));
#68665=CARTESIAN_POINT('Ctrl Pts',(-26.6061399701061,26.0288593521594,-65.9813522577802));
#68666=CARTESIAN_POINT('Ctrl Pts',(-26.5304585140938,26.1167406580002,-65.9872037629225));
#68667=CARTESIAN_POINT('Ctrl Pts',(-26.4547519259174,26.2046511473096,-65.9930572112223));
#68668=CARTESIAN_POINT('Ctrl Pts',(-26.3751830156822,26.289173301837,-65.998910659522));
#68669=CARTESIAN_POINT('Ctrl Pts',(-26.2920980699472,26.3699638723038,-66.0047641078218));
#68670=CARTESIAN_POINT('Ctrl Pts',(-26.2089186385874,26.4508463191924,-66.0106242127633));
#68671=CARTESIAN_POINT('Ctrl Pts',(-26.122215487396,26.5279884235244,-66.0164843177048));
#68672=CARTESIAN_POINT('Ctrl Pts',(-26.0323696951043,26.6010857600279,-66.0223444226463));
#68673=CARTESIAN_POINT('Ctrl Pts',(-25.9424633972947,26.6742323230125,-66.0282084740017));
#68674=CARTESIAN_POINT('Ctrl Pts',(-25.8494105753464,26.7433284485053,-66.0340725253572));
#68675=CARTESIAN_POINT('Ctrl Pts',(-25.7536216866102,26.8081127753457,-66.0399365767126));
#68676=CARTESIAN_POINT('Ctrl Pts',(-25.6576916241731,26.8729925813517,-66.0458092705091));
#68677=CARTESIAN_POINT('Ctrl Pts',(-25.5590177980276,26.9335476904816,-66.0516819643057));
#68678=CARTESIAN_POINT('Ctrl Pts',(-25.458035720091,26.9895623906733,-66.0575546581023));
#68679=CARTESIAN_POINT('Ctrl Pts',(-25.430388516378,27.004898278573,-66.0591625034255));
#68680=CARTESIAN_POINT('Ctrl Pts',(-25.4025684081857,27.0198941081355,-66.0607703487487));
#68681=CARTESIAN_POINT('Ctrl Pts',(-25.3745845778111,27.034546087856,-66.0623781940719));
#68682=CARTESIAN_POINT('Ctrl Pts',(-25.2723798694919,27.0880591807242,-66.0682504910406));
#68683=CARTESIAN_POINT('Ctrl Pts',(-25.1676473967304,27.1371611570424,-66.0741227880092));
#68684=CARTESIAN_POINT('Ctrl Pts',(-25.0608046435372,27.181605078254,-66.0799950849779));
#68685=CARTESIAN_POINT('Ctrl Pts',(-24.9541003500669,27.2259914036735,-66.0858597719161));
#68686=CARTESIAN_POINT('Ctrl Pts',(-24.8452915927674,27.2657315210544,-66.0917244588543));
#68687=CARTESIAN_POINT('Ctrl Pts',(-24.7348207964185,27.3006241167786,-66.0975891457925));
#68688=CARTESIAN_POINT('Ctrl Pts',(-24.6244636123681,27.3354808276523,-66.1034478012673));
#68689=CARTESIAN_POINT('Ctrl Pts',(-24.5124481809777,27.3654998092747,-66.1093064567421));
#68690=CARTESIAN_POINT('Ctrl Pts',(-24.3992366495488,27.3905279082305,-66.1151651122169));
#68691=CARTESIAN_POINT('Ctrl Pts',(-24.2816029759865,27.4165336267759,-66.1212526119348));
#68692=CARTESIAN_POINT('Ctrl Pts',(-24.162678275845,27.4371504430135,-66.1273401116528));
#68693=CARTESIAN_POINT('Ctrl Pts',(-24.0429984641129,27.4522636088293,-66.1334276113707));
#68694=CARTESIAN_POINT('Ctrl Pts',(-23.9279511142459,27.466791787392,-66.1392794814541));
#68695=CARTESIAN_POINT('Ctrl Pts',(-23.8122064706178,27.4762343976616,-66.1451313515375));
#68696=CARTESIAN_POINT('Ctrl Pts',(-23.696249908617,27.4805418042455,-66.1509832216209));
#68697=CARTESIAN_POINT('Ctrl Pts',(-23.5803110020571,27.4848485549875,-66.1568342007039));
#68698=CARTESIAN_POINT('Ctrl Pts',(-23.4641606542651,27.4840216413335,-66.1626851797869));
#68699=CARTESIAN_POINT('Ctrl Pts',(-23.348286931179,27.4780634864384,-66.1685361588699));
#68700=CARTESIAN_POINT('Ctrl Pts',(-23.2324027899302,27.4721047958478,-66.1743876640122));
#68701=CARTESIAN_POINT('Ctrl Pts',(-23.1167957356909,27.4610139681281,-66.1802391691545));
#68702=CARTESIAN_POINT('Ctrl Pts',(-23.0019506832539,27.444845460743,-66.1860906742968));
#68703=CARTESIAN_POINT('Ctrl Pts',(-22.887067493275,27.4286715841485,-66.1919441225965));
#68704=CARTESIAN_POINT('Ctrl Pts',(-22.7729472173903,27.4074167326116,-66.1977975708963));
#68705=CARTESIAN_POINT('Ctrl Pts',(-22.6600658195423,27.3811867020381,-66.2036510191961));
#68706=CARTESIAN_POINT('Ctrl Pts',(-22.5470560510331,27.354926842224,-66.2095111241376));
#68707=CARTESIAN_POINT('Ctrl Pts',(-22.4352883755231,27.3236806040775,-66.2153712290792));
#68708=CARTESIAN_POINT('Ctrl Pts',(-22.3252249003106,27.287604040764,-66.2212313340208));
#68709=CARTESIAN_POINT('Ctrl Pts',(-22.2150873042362,27.2515031821432,-66.2270953853762));
#68710=CARTESIAN_POINT('Ctrl Pts',(-22.1066565794953,27.2105656667968,-66.2329594367317));
#68711=CARTESIAN_POINT('Ctrl Pts',(-22.000374483216,27.1649955425935,-66.2388234880871));
#68712=CARTESIAN_POINT('Ctrl Pts',(-21.8939357483426,27.1193582571238,-66.2446961818837));
#68713=CARTESIAN_POINT('Ctrl Pts',(-21.7896523329111,27.0690749152121,-66.2505688756803));
#68714=CARTESIAN_POINT('Ctrl Pts',(-21.6879411317527,27.0143953188275,-66.2564415694769));
#68715=CARTESIAN_POINT('Ctrl Pts',(-21.6600943062949,26.9994249600147,-66.2580494148003));
#68716=CARTESIAN_POINT('Ctrl Pts',(-21.632440115421,26.984125317815,-66.2596572601237));
#68717=CARTESIAN_POINT('Ctrl Pts',(-21.6049867124081,26.9685020679799,-66.2612651054471));
#68718=CARTESIAN_POINT('Ctrl Pts',(-21.5047192719105,26.9114416273313,-66.2671374024158));
#68719=CARTESIAN_POINT('Ctrl Pts',(-21.4067966139366,26.8498701405502,-66.2730096993845));
#68720=CARTESIAN_POINT('Ctrl Pts',(-21.3116521598433,26.784005363181,-66.2788819963532));
#68721=CARTESIAN_POINT('Ctrl Pts',(-21.2166310054064,26.7182259413325,-66.2847466832914));
#68722=CARTESIAN_POINT('Ctrl Pts',(-21.1243812318333,26.6481645263437,-66.2906113702296));
#68723=CARTESIAN_POINT('Ctrl Pts',(-21.0353113569978,26.57408451906,-66.2964760571678));
#68724=CARTESIAN_POINT('Ctrl Pts',(-20.9463330849527,26.5000806984263,-66.3023347126426));
#68725=CARTESIAN_POINT('Ctrl Pts',(-20.86052852271,26.4220667687367,-66.3081933681175));
#68726=CARTESIAN_POINT('Ctrl Pts',(-20.778276331016,26.3403487563563,-66.3140520235923));
#68727=CARTESIAN_POINT('Ctrl Pts',(-20.6928112962676,26.2554387664361,-66.3201395233102));
#68728=CARTESIAN_POINT('Ctrl Pts',(-20.6111821808506,26.1665296840443,-66.3262270230281));
#68729=CARTESIAN_POINT('Ctrl Pts',(-20.5337752090489,26.0740103572326,-66.332314522746));
#68730=CARTESIAN_POINT('Ctrl Pts',(-20.4593644388601,25.9850721879029,-66.3381663928294));
#68731=CARTESIAN_POINT('Ctrl Pts',(-20.3888553257652,25.8927984083777,-66.3440182629128));
#68732=CARTESIAN_POINT('Ctrl Pts',(-20.3225519948264,25.7975705430809,-66.3498701329962));
#68733=CARTESIAN_POINT('Ctrl Pts',(-20.2562587591726,25.7023571770926,-66.3557211120791));
#68734=CARTESIAN_POINT('Ctrl Pts',(-20.1941702685596,25.6041909588105,-66.3615720911621));
#68735=CARTESIAN_POINT('Ctrl Pts',(-20.1365483046765,25.5034838161153,-66.367423070245));
#68736=CARTESIAN_POINT('Ctrl Pts',(-20.0789211600242,25.4027676188787,-66.3732745753873));
#68737=CARTESIAN_POINT('Ctrl Pts',(-20.0257615457222,25.2995104019073,-66.3791260805296));
#68738=CARTESIAN_POINT('Ctrl Pts',(-19.9772857627949,25.1941495687198,-66.3849775856719));
#68739=CARTESIAN_POINT('Ctrl Pts',(-19.9287938821155,25.0887537474933,-66.3908310339717));
#68740=CARTESIAN_POINT('Ctrl Pts',(-19.884989098315,24.9812532963402,-66.3966844822715));
#68741=CARTESIAN_POINT('Ctrl Pts',(-19.8460396822115,24.8721058388836,-66.4025379305712));
#68742=CARTESIAN_POINT('Ctrl Pts',(-19.8070459721642,24.7628342570669,-66.4083980355127));
#68743=CARTESIAN_POINT('Ctrl Pts',(-19.7729187897928,24.6519123200544,-66.4142581404543));
#68744=CARTESIAN_POINT('Ctrl Pts',(-19.7437766335357,24.5398131598208,-66.4201182453958));
#68745=CARTESIAN_POINT('Ctrl Pts',(-19.7146148518602,24.4276385078188,-66.4259822967512));
#68746=CARTESIAN_POINT('Ctrl Pts',(-19.6904448669539,24.3142854573075,-66.4318463481067));
#68747=CARTESIAN_POINT('Ctrl Pts',(-19.6713337983761,24.2002359624937,-66.4377103994621));
#68748=CARTESIAN_POINT('Ctrl Pts',(-19.6521945638982,24.086018381491,-66.4435830932587));
#68749=CARTESIAN_POINT('Ctrl Pts',(-19.6381291761864,23.9711027164301,-66.4494557870552));
#68750=CARTESIAN_POINT('Ctrl Pts',(-19.6291528219826,23.8559747364813,-66.4553284808518));
#68751=CARTESIAN_POINT('Ctrl Pts',(-19.6266952463577,23.8244546214269,-66.4569363261751));
#68752=CARTESIAN_POINT('Ctrl Pts',(-19.6246188295299,23.7929185814501,-66.4585441714985));
#68753=CARTESIAN_POINT('Ctrl Pts',(-19.6229232035861,23.7613765440241,-66.4601520168218));
#68754=CARTESIAN_POINT('Ctrl Pts',(-19.6167303074505,23.6461762768871,-66.4660243137905));
#68755=CARTESIAN_POINT('Ctrl Pts',(-19.61560008447,23.5305103029573,-66.4718966107592));
#68756=CARTESIAN_POINT('Ctrl Pts',(-19.6195836158691,23.4148609729973,-66.4777689077279));
#68757=CARTESIAN_POINT('Ctrl Pts',(-19.6235619849278,23.2993615153842,-66.4836335946661));
#68758=CARTESIAN_POINT('Ctrl Pts',(-19.6326409155039,23.183879068172,-66.4894982816044));
#68759=CARTESIAN_POINT('Ctrl Pts',(-19.6468196252758,23.0688997036252,-66.4953629685426));
#68760=CARTESIAN_POINT('Ctrl Pts',(-19.6609837531323,22.9540385881571,-66.5012216240174));
#68761=CARTESIAN_POINT('Ctrl Pts',(-19.6802371777114,22.8396799340498,-66.5070802794922));
#68762=CARTESIAN_POINT('Ctrl Pts',(-19.7045271160835,22.7263077351659,-66.512938934967));
#68763=CARTESIAN_POINT('Ctrl Pts',(-19.7297658408427,22.6085071183368,-66.5190264346849));
#68764=CARTESIAN_POINT('Ctrl Pts',(-19.7604425462107,22.4917720457867,-66.5251139344028));
#68765=CARTESIAN_POINT('Ctrl Pts',(-19.7964388583962,22.3766376433423,-66.5312014341207));
#68766=CARTESIAN_POINT('Ctrl Pts',(-19.8310418566964,22.2659597630209,-66.5370533042041));
#68767=CARTESIAN_POINT('Ctrl Pts',(-19.870560170882,22.1567613735582,-66.5429051742875));
#68768=CARTESIAN_POINT('Ctrl Pts',(-19.9148372105427,22.0495045705971,-66.5487570443709));
#68769=CARTESIAN_POINT('Ctrl Pts',(-19.9591075086215,21.9422640984595,-66.5546080234539));
#68770=CARTESIAN_POINT('Ctrl Pts',(-20.008134933825,21.8369650070279,-66.5604590025369));
#68771=CARTESIAN_POINT('Ctrl Pts',(-20.0617144284166,21.7340502021118,-66.5663099816199));
#68772=CARTESIAN_POINT('Ctrl Pts',(-20.1152987403204,21.6311261441644,-66.5721614867622));
#68773=CARTESIAN_POINT('Ctrl Pts',(-20.1734357443073,21.5305871655698,-66.5780129919045));
#68774=CARTESIAN_POINT('Ctrl Pts',(-20.2358743653315,21.4328516791539,-66.5838644970468));
#68775=CARTESIAN_POINT('Ctrl Pts',(-20.2983337208625,21.3350837369106,-66.5897179453465));
#68776=CARTESIAN_POINT('Ctrl Pts',(-20.365097311426,21.240121486216,-66.5955713936463));
#68777=CARTESIAN_POINT('Ctrl Pts',(-20.4358710881004,21.1483538611007,-66.6014248419461));
#68778=CARTESIAN_POINT('Ctrl Pts',(-20.5067253499271,21.0564818762688,-66.6072849468876));
#68779=CARTESIAN_POINT('Ctrl Pts',(-20.5815986477857,20.9678120958755,-66.6131450518292));
#68780=CARTESIAN_POINT('Ctrl Pts',(-20.660156981237,20.8826999625351,-66.6190051567707));
#68781=CARTESIAN_POINT('Ctrl Pts',(-20.738768218809,20.7975305114998,-66.6248692081262));
#68782=CARTESIAN_POINT('Ctrl Pts',(-20.8210691405895,20.7159237684898,-66.6307332594816));
#68783=CARTESIAN_POINT('Ctrl Pts',(-20.906690551385,20.638196718997,-66.6365973108371));
#68784=CARTESIAN_POINT('Ctrl Pts',(-20.9924381510483,20.560355115349,-66.6424700046337));
#68785=CARTESIAN_POINT('Ctrl Pts',(-21.0815156898151,20.4864048800883,-66.6483426984303));
#68786=CARTESIAN_POINT('Ctrl Pts',(-21.17352269101,20.4166213689054,-66.6542153922268));
#68787=CARTESIAN_POINT('Ctrl Pts',(-21.198712668848,20.3975158108791,-66.6558232375502));
#68788=CARTESIAN_POINT('Ctrl Pts',(-21.2241220770787,20.3787223200483,-66.6574310828735));
#68789=CARTESIAN_POINT('Ctrl Pts',(-21.2497423646799,20.3602459531016,-66.6590389281968));
#68790=CARTESIAN_POINT('Ctrl Pts',(-21.3433147593839,20.2927651376033,-66.6649112251655));
#68791=CARTESIAN_POINT('Ctrl Pts',(-21.4400155504888,20.229291899709,-66.6707835221342));
#68792=CARTESIAN_POINT('Ctrl Pts',(-21.5394665397721,20.1701299459453,-66.6766558191029));
#68793=CARTESIAN_POINT('Ctrl Pts',(-21.6387886484716,20.1110446613751,-66.6825205060411));
#68794=CARTESIAN_POINT('Ctrl Pts',(-21.7408535157637,20.0562597596307,-66.6883851929793));
#68795=CARTESIAN_POINT('Ctrl Pts',(-21.8452517780188,20.0060373251969,-66.6942498799175));
#68796=CARTESIAN_POINT('Ctrl Pts',(-21.9495426731966,19.9558665413931,-66.7001085353923));
#68797=CARTESIAN_POINT('Ctrl Pts',(-22.0561618198304,19.9102490699777,-66.7059671908672));
#68798=CARTESIAN_POINT('Ctrl Pts',(-22.1646734943517,19.8694021229874,-66.711825846342));
#68799=CARTESIAN_POINT('Ctrl Pts',(-22.2774237304557,19.8269596582701,-66.7179133460599));
#68800=CARTESIAN_POINT('Ctrl Pts',(-22.3922169653313,19.7896682297332,-66.7240008457778));
#68801=CARTESIAN_POINT('Ctrl Pts',(-22.5085390025895,19.7577175057148,-66.7300883454957));
#68802=CARTESIAN_POINT('Ctrl Pts',(-22.6203585477911,19.7270035024803,-66.7359402155791));
#68803=CARTESIAN_POINT('Ctrl Pts',(-22.7335903091212,19.7012245644998,-66.7417920856625));
#68804=CARTESIAN_POINT('Ctrl Pts',(-22.847760874007,19.6804987319183,-66.7476439557459));
#68805=CARTESIAN_POINT('Ctrl Pts',(-22.9619140553862,19.6597760550333,-66.7534949348288));
#68806=CARTESIAN_POINT('Ctrl Pts',(-23.0770053494842,19.6441050275871,-66.7593459139118));
#68807=CARTESIAN_POINT('Ctrl Pts',(-23.1925512898128,19.6335525404316,-66.7651968929947));
#68808=CARTESIAN_POINT('Ctrl Pts',(-23.3081076188334,19.6229991045059,-66.771048398137));
#68809=CARTESIAN_POINT('Ctrl Pts',(-23.4241182636503,19.6175651613169,-66.7768999032793));
#68810=CARTESIAN_POINT('Ctrl Pts',(-23.5400954898268,19.617265647086,-66.7827514084216));
#68811=CARTESIAN_POINT('Ctrl Pts',(-23.6561112295153,19.6169660333929,-66.7886048567214));
#68812=CARTESIAN_POINT('Ctrl Pts',(-23.7720931153339,19.6218042400739,-66.7944583050212));
#68813=CARTESIAN_POINT('Ctrl Pts',(-23.8875549846491,19.6317431141694,-66.8003117533209));
#68814=CARTESIAN_POINT('Ctrl Pts',(-24.0031481591818,19.6416932909229,-66.8061718582625));
#68815=CARTESIAN_POINT('Ctrl Pts',(-24.1182197247471,19.6567556773726,-66.812031963204));
#68816=CARTESIAN_POINT('Ctrl Pts',(-24.2322901001133,19.6768414051463,-66.8178920681455));
#68817=CARTESIAN_POINT('Ctrl Pts',(-24.3464372947379,19.6969406594005,-66.823756119501));
#68818=CARTESIAN_POINT('Ctrl Pts',(-24.4595815540564,19.7220699016073,-66.8296201708564));
#68819=CARTESIAN_POINT('Ctrl Pts',(-24.5712566272026,19.7520898657523,-66.8354842222119));
#68820=CARTESIAN_POINT('Ctrl Pts',(-24.683096287114,19.7821540733318,-66.8413569160084));
#68821=CARTESIAN_POINT('Ctrl Pts',(-24.7934620467624,19.8171232641298,-66.847229609805));
#68822=CARTESIAN_POINT('Ctrl Pts',(-24.901905770165,19.8568093518238,-66.8531023036016));
#68823=CARTESIAN_POINT('Ctrl Pts',(-24.9315958475913,19.8676747387674,-66.8547101489249));
#68824=CARTESIAN_POINT('Ctrl Pts',(-24.9611419890797,19.8788934217309,-66.8563179942483));
#68825=CARTESIAN_POINT('Ctrl Pts',(-24.9905353181631,19.89046093995,-66.8579258395717));
#68826=CARTESIAN_POINT('Ctrl Pts',(-25.0978879066045,19.9327087241036,-66.8637981365404));
#68827=CARTESIAN_POINT('Ctrl Pts',(-25.2035598836444,19.9797547462265,-66.869670433509));
#68828=CARTESIAN_POINT('Ctrl Pts',(-25.3070913037141,20.0314449880613,-66.8755427304777));
#68829=CARTESIAN_POINT('Ctrl Pts',(-25.4104885552857,20.0830682434479,-66.8814074174159));
#68830=CARTESIAN_POINT('Ctrl Pts',(-25.5117503999262,20.1393235668807,-66.8872721043542));
#68831=CARTESIAN_POINT('Ctrl Pts',(-25.6104350631652,20.2000082216443,-66.8931367912924));
#68832=CARTESIAN_POINT('Ctrl Pts',(-25.7090182354057,20.2606304660393,-66.8989954467672));
#68833=CARTESIAN_POINT('Ctrl Pts',(-25.8050291481507,20.3256727658229,-66.904854102242));
#68834=CARTESIAN_POINT('Ctrl Pts',(-25.8980495302091,20.3948859517602,-66.9107127577169));
#68835=CARTESIAN_POINT('Ctrl Pts',(-25.9947033703219,20.4668026657023,-66.9168002574348));
#68836=CARTESIAN_POINT('Ctrl Pts',(-26.0881278847157,20.5432225422124,-66.9228877571526));
#68837=CARTESIAN_POINT('Ctrl Pts',(-26.1778855572887,20.6238155030183,-66.9289752568705));
#68838=CARTESIAN_POINT('Ctrl Pts',(-26.2641689680855,20.7012889417252,-66.9348271269539));
#68839=CARTESIAN_POINT('Ctrl Pts',(-26.3470637883679,20.7826181135374,-66.9406789970374));
#68840=CARTESIAN_POINT('Ctrl Pts',(-26.4262148094164,20.8674685342172,-66.9465308671208));
#68841=CARTESIAN_POINT('Ctrl Pts',(-26.5053537790023,20.9523060356488,-66.9523818462037));
#68842=CARTESIAN_POINT('Ctrl Pts',(-26.5807498008514,21.040663417727,-66.9582328252867));
#68843=CARTESIAN_POINT('Ctrl Pts',(-26.6520852644353,21.1321700893246,-66.9640838043697));
#68844=CARTESIAN_POINT('Ctrl Pts',(-26.7234271417638,21.2236849882525,-66.969935309512));
#68845=CARTESIAN_POINT('Ctrl Pts',(-26.7907074809046,21.3183494135374,-66.9757868146542));
#68846=CARTESIAN_POINT('Ctrl Pts',(-26.8536500746243,21.415761099675,-66.9816383197965));
#68847=CARTESIAN_POINT('Ctrl Pts',(-26.9166135702093,21.5132051341132,-66.9874917680963));
#68848=CARTESIAN_POINT('Ctrl Pts',(-26.975236231858,21.6133978964424,-66.9933452163961));
#68849=CARTESIAN_POINT('Ctrl Pts',(-27.0292865254656,21.7159102871326,-66.9991986646959));
#68850=CARTESIAN_POINT('Ctrl Pts',(-27.0833982859936,21.818539256671,-67.0050587696374));
#68851=CARTESIAN_POINT('Ctrl Pts',(-27.132927106971,21.9234927538961,-67.0109188745789));
#68852=CARTESIAN_POINT('Ctrl Pts',(-27.1776885208635,22.0303192619487,-67.0167789795205));
#68853=CARTESIAN_POINT('Ctrl Pts',(-27.2224800787668,22.1372177109685,-67.0226430308759));
#68854=CARTESIAN_POINT('Ctrl Pts',(-27.2624976943609,22.2459912954124,-67.0285070822314));
#68855=CARTESIAN_POINT('Ctrl Pts',(-27.2976065061211,22.3561724714191,-67.0343711335868));
#68856=CARTESIAN_POINT('Ctrl Pts',(-27.3327670612616,22.4665160324851,-67.0402438273834));
#68857=CARTESIAN_POINT('Ctrl Pts',(-27.3630042661482,22.578270927897,-67.04611652118));
#68858=CARTESIAN_POINT('Ctrl Pts',(-27.3882341244631,22.6909584647025,-67.0519892149766));
#68859=CARTESIAN_POINT('Ctrl Pts',(-27.3951416376258,22.7218104272479,-67.0535970602999));
#68860=CARTESIAN_POINT('Ctrl Pts',(-27.4016741134431,22.7527322655498,-67.0552049056232));
#68861=CARTESIAN_POINT('Ctrl Pts',(-27.4078305067238,22.7837141004552,-67.0568127509466));
#68862=CARTESIAN_POINT('Ctrl Pts',(-27.440427587772,22.9477577762541,-67.065326025185));
#68863=CARTESIAN_POINT('Ctrl Pts',(-27.4625690874079,23.1139424991538,-67.0738392994233));
#68864=CARTESIAN_POINT('Ctrl Pts',(-27.4740372302633,23.2811751464035,-67.0823525736617));
#68865=CARTESIAN_POINT('Ctrl Pts',(-27.480091905839,23.3694666367974,-67.0868472084295));
#68866=CARTESIAN_POINT('Ctrl Pts',(-27.4831722163398,23.4580498634429,-67.0913418431973));
#68867=CARTESIAN_POINT('Ctrl Pts',(-27.4832509814148,23.5467604699193,-67.0958364779651));
#68868=CARTESIAN_POINT('',(-27.4767668984626,23.5498433970659,-68.3458364779651));
#68869=CARTESIAN_POINT('Ctrl Pts',(-27.4847103606465,23.5467734800025,-67.0958372025195));
#68870=CARTESIAN_POINT('Ctrl Pts',(-27.4749839165426,24.5989084225538,-67.1491246891201));
#68871=CARTESIAN_POINT('Ctrl Pts',(-26.4981045555357,26.9759418482296,-67.2687078128457));
#68872=CARTESIAN_POINT('Ctrl Pts',(-22.4784874858222,28.077069351332,-67.4545865736964));
#68873=CARTESIAN_POINT('Ctrl Pts',(-19.1624311466427,25.0954950126635,-67.6534734850713));
#68874=CARTESIAN_POINT('Ctrl Pts',(-19.8784106344222,20.6939738489423,-67.852360396446));
#68875=CARTESIAN_POINT('Ctrl Pts',(-23.968501504941,18.9171306221722,-68.051247307821));
#68876=CARTESIAN_POINT('Ctrl Pts',(-27.0333951896357,20.9687458373182,-68.215739334994));
#68877=CARTESIAN_POINT('Ctrl Pts',(-27.4773521810207,22.9167498443613,-68.313935725042));
#68878=CARTESIAN_POINT('Ctrl Pts',(-27.4767668984626,23.5498433970659,-68.3458364779651));
#68879=CARTESIAN_POINT('',(-27.4832039003184,23.5538862193999,-69.5958364779651));
#68880=CARTESIAN_POINT('Ctrl Pts',(-27.4767668984626,23.5498433970659,-68.3458364779651));
#68881=CARTESIAN_POINT('Ctrl Pts',(-27.4761358561213,24.2324347919078,-68.380231362167));
#68882=CARTESIAN_POINT('Ctrl Pts',(-26.9814714499248,26.231567390239,-68.4809218834938));
#68883=CARTESIAN_POINT('Ctrl Pts',(-23.7939922423769,28.1958248092063,-68.6479080419455));
#68884=CARTESIAN_POINT('Ctrl Pts',(-19.7736062765533,26.2664435955882,-68.8467949533207));
#68885=CARTESIAN_POINT('Ctrl Pts',(-19.2236380124017,21.8411130893086,-69.0456818646953));
#68886=CARTESIAN_POINT('Ctrl Pts',(-22.649461655072,18.9863368193928,-69.2445687760705));
#68887=CARTESIAN_POINT('Ctrl Pts',(-26.5714951847596,20.2210392543588,-69.4279536471601));
#68888=CARTESIAN_POINT('Ctrl Pts',(-27.4739245090166,22.5500065074999,-69.5450428811251));
#68889=CARTESIAN_POINT('Ctrl Pts',(-27.4832039003184,23.5538862193999,-69.5958364779651));
#68890=CARTESIAN_POINT('',(-27.4892926031819,23.5490236752345,-70.845836477965));
#68891=CARTESIAN_POINT('Ctrl Pts',(-27.4832039003184,23.5538862193999,-69.5958364779651));
#68892=CARTESIAN_POINT('Ctrl Pts',(-27.4860359403141,23.8602670371284,-69.6113385182501));
#68893=CARTESIAN_POINT('Ctrl Pts',(-27.313134779593,25.4737471440459,-69.6931361956599));
#68894=CARTESIAN_POINT('Ctrl Pts',(-25.08984694793,27.9400588904566,-69.841229510195));
#68895=CARTESIAN_POINT('Ctrl Pts',(-20.6892508390938,27.2184155792749,-70.0401164215698));
#68896=CARTESIAN_POINT('Ctrl Pts',(-18.9176727125942,23.1260414377581,-70.2390033329449));
#68897=CARTESIAN_POINT('Ctrl Pts',(-21.4030426622697,19.4234813216558,-70.4378902443196));
#68898=CARTESIAN_POINT('Ctrl Pts',(-25.8615164277807,19.51307406026,-70.6367771556946));
#68899=CARTESIAN_POINT('Ctrl Pts',(-27.4577312464195,22.110794924436,-70.7727592335762));
#68900=CARTESIAN_POINT('Ctrl Pts',(-27.4895653266935,23.4822771529814,-70.8424456743331));
#68901=CARTESIAN_POINT('Ctrl Pts',(-27.4892926031819,23.5490236752345,-70.845836477965));
#68902=CARTESIAN_POINT('',(-27.4821474792635,23.5472069989156,-72.0958360514227));
#68903=CARTESIAN_POINT('Ctrl Pts',(-27.4892926031819,23.5490236752345,-70.845836477965));
#68904=CARTESIAN_POINT('Ctrl Pts',(-27.4842331456164,24.7872784739266,-70.9087413114581));
#68905=CARTESIAN_POINT('Ctrl Pts',(-26.1861220606148,27.3396704490119,-71.0379417820763));
#68906=CARTESIAN_POINT('Ctrl Pts',(-21.835546490849,27.8746639197317,-71.2334378898192));
#68907=CARTESIAN_POINT('Ctrl Pts',(-18.9851813454571,24.4451692930999,-71.4323248011941));
#68908=CARTESIAN_POINT('Ctrl Pts',(-20.3297295849991,20.1933219148442,-71.6312117125691));
#68909=CARTESIAN_POINT('Ctrl Pts',(-24.6336653213793,19.0262093874363,-71.8300986239438));
#68910=CARTESIAN_POINT('Ctrl Pts',(-27.2099139446467,21.3546175314318,-71.9849730572581));
#68911=CARTESIAN_POINT('Ctrl Pts',(-27.4826159325481,23.1057213294587,-72.0735518534471));
#68912=CARTESIAN_POINT('Ctrl Pts',(-27.4794588064285,23.5471884932199,-72.0958350125112));
#68913=CARTESIAN_POINT('',(-27.481501086808,23.5526898751615,-73.3458370071997));
#68914=CARTESIAN_POINT('Ctrl Pts',(-27.4832513584104,23.5472145967353,-72.095836477965));
#68915=CARTESIAN_POINT('Ctrl Pts',(-27.4833409718037,23.6632306982906,-72.1016868061657));
#68916=CARTESIAN_POINT('Ctrl Pts',(-27.4782928946537,23.7793051745592,-72.1075371343664));
#68917=CARTESIAN_POINT('Ctrl Pts',(-27.4681183761652,23.8949498260379,-72.113387462567));
#68918=CARTESIAN_POINT('Ctrl Pts',(-27.457945360829,24.0105773925284,-72.119236926458));
#68919=CARTESIAN_POINT('Ctrl Pts',(-27.4426474459296,24.1257748492107,-72.1250863903491));
#68920=CARTESIAN_POINT('Ctrl Pts',(-27.4222878729755,24.2400578055713,-72.1309358542401));
#68921=CARTESIAN_POINT('Ctrl Pts',(-27.4019263907767,24.3543514789602,-72.136785866672));
#68922=CARTESIAN_POINT('Ctrl Pts',(-27.3765023790015,24.4677300748901,-72.1426358791038));
#68923=CARTESIAN_POINT('Ctrl Pts',(-27.346130322552,24.5797187996565,-72.1484858915357));
#68924=CARTESIAN_POINT('Ctrl Pts',(-27.3157480826565,24.6917450731197,-72.1543378654181));
#68925=CARTESIAN_POINT('Ctrl Pts',(-27.2804146068323,24.8023801502962,-72.1601898393005));
#68926=CARTESIAN_POINT('Ctrl Pts',(-27.2402942145768,24.9111644974689,-72.1660418131829));
#68927=CARTESIAN_POINT('Ctrl Pts',(-27.2001256652783,25.0200794199474,-72.1719008112678));
#68928=CARTESIAN_POINT('Ctrl Pts',(-27.1551588714224,25.1271387895848,-72.1777598093527));
#68929=CARTESIAN_POINT('Ctrl Pts',(-27.1056063485421,25.2319029820035,-72.1836188074376));
#68930=CARTESIAN_POINT('Ctrl Pts',(-27.0560204868967,25.3367376594064,-72.1894817474359));
#68931=CARTESIAN_POINT('Ctrl Pts',(-27.0018429450793,25.4392737202483,-72.1953446874343));
#68932=CARTESIAN_POINT('Ctrl Pts',(-26.9433313556434,25.5390976977309,-72.2012076274327));
#68933=CARTESIAN_POINT('Ctrl Pts',(-26.8847251742034,25.6390830543552,-72.2070800456772));
#68934=CARTESIAN_POINT('Ctrl Pts',(-26.8217711792399,25.7363472275307,-72.2129524639217));
#68935=CARTESIAN_POINT('Ctrl Pts',(-26.7547694728672,25.830506941565,-72.2188248821662));
#68936=CARTESIAN_POINT('Ctrl Pts',(-26.7203598970834,25.8788638565042,-72.2218407370087));
#68937=CARTESIAN_POINT('Ctrl Pts',(-26.6848833939656,25.9264025322493,-72.2248565918512));
#68938=CARTESIAN_POINT('Ctrl Pts',(-26.6483844666265,25.9730747525252,-72.2278724466937));
#68939=CARTESIAN_POINT('Ctrl Pts',(-26.5773158620215,26.0639522059367,-72.2337447451685));
#68940=CARTESIAN_POINT('Ctrl Pts',(-26.5021262477415,26.1518522713299,-72.2396170436432));
#68941=CARTESIAN_POINT('Ctrl Pts',(-26.4230942404892,26.2363779040862,-72.2454893421181));
#68942=CARTESIAN_POINT('Ctrl Pts',(-26.3441646528039,26.3207939979479,-72.2513540305335));
#68943=CARTESIAN_POINT('Ctrl Pts',(-26.261402854215,26.401844056358,-72.257218718949));
#68944=CARTESIAN_POINT('Ctrl Pts',(-26.1751289884192,26.4791623266402,-72.2630834073644));
#68945=CARTESIAN_POINT('Ctrl Pts',(-26.0889438503148,26.5564010795442,-72.2689420642863));
#68946=CARTESIAN_POINT('Ctrl Pts',(-25.9992541353705,26.6299154039258,-72.2748007212082));
#68947=CARTESIAN_POINT('Ctrl Pts',(-25.9064178045803,26.6993752995211,-72.2806593781302));
#68948=CARTESIAN_POINT('Ctrl Pts',(-25.8099552375422,26.7715483354251,-72.2867468772942));
#68949=CARTESIAN_POINT('Ctrl Pts',(-25.7100955370243,26.8393434171954,-72.2928343764584));
#68950=CARTESIAN_POINT('Ctrl Pts',(-25.6072797030729,26.9024351365369,-72.2989218756225));
#68951=CARTESIAN_POINT('Ctrl Pts',(-25.5084435428034,26.9630847762359,-72.3047737470697));
#68952=CARTESIAN_POINT('Ctrl Pts',(-25.4068762241754,27.0193881513439,-72.3106256185169));
#68953=CARTESIAN_POINT('Ctrl Pts',(-25.3029995332083,27.0711000076129,-72.3164774899641));
#68954=CARTESIAN_POINT('Ctrl Pts',(-25.1991386589906,27.1228039899936,-72.3223284703781));
#68955=CARTESIAN_POINT('Ctrl Pts',(-25.0929694815596,27.1699176594476,-72.3281794507921));
#68956=CARTESIAN_POINT('Ctrl Pts',(-24.984937692417,27.2122420851476,-72.3340304312061));
#68957=CARTESIAN_POINT('Ctrl Pts',(-24.8768961908077,27.2545703159736,-72.3398819376454));
#68958=CARTESIAN_POINT('Ctrl Pts',(-24.7669921295208,27.2921082963066,-72.3457334440847));
#68959=CARTESIAN_POINT('Ctrl Pts',(-24.6556897729954,27.324705804096,-72.3515849505239));
#68960=CARTESIAN_POINT('Ctrl Pts',(-24.5443504560599,27.357314136609,-72.3574384000854));
#68961=CARTESIAN_POINT('Ctrl Pts',(-24.4316123170939,27.3849786182353,-72.3632918496468));
#68962=CARTESIAN_POINT('Ctrl Pts',(-24.3179526224015,27.4075994918117,-72.3691452992083));
#68963=CARTESIAN_POINT('Ctrl Pts',(-24.2041636731156,27.4302460900025,-72.3750054053532));
#68964=CARTESIAN_POINT('Ctrl Pts',(-24.0894514819994,27.4478375512691,-72.3808655114981));
#68965=CARTESIAN_POINT('Ctrl Pts',(-23.9743014018211,27.4603256199809,-72.386725617643));
#68966=CARTESIAN_POINT('Ctrl Pts',(-23.8590737759236,27.4728220985546,-72.3925896701694));
#68967=CARTESIAN_POINT('Ctrl Pts',(-23.7434080853169,27.480208314969,-72.3984537226958));
#68968=CARTESIAN_POINT('Ctrl Pts',(-23.6277909203501,27.4824881297077,-72.4043177752222));
#68969=CARTESIAN_POINT('Ctrl Pts',(-23.5120033599067,27.4847713044157,-72.4101904701333));
#68970=CARTESIAN_POINT('Ctrl Pts',(-23.3962648795434,27.4819330675668,-72.4160631650445));
#68971=CARTESIAN_POINT('Ctrl Pts',(-23.2810582726591,27.4740292137828,-72.4219358599556));
#68972=CARTESIAN_POINT('Ctrl Pts',(-23.2495168844031,27.4718652882263,-72.4235436926599));
#68973=CARTESIAN_POINT('Ctrl Pts',(-23.2180153091037,27.4693219604832,-72.4251515253643));
#68974=CARTESIAN_POINT('Ctrl Pts',(-23.1865633142998,27.4664010417933,-72.4267593580686));
#68975=CARTESIAN_POINT('Ctrl Pts',(-23.0716907827328,27.4557329322979,-72.4326316664621));
#68976=CARTESIAN_POINT('Ctrl Pts',(-22.9570956039099,27.4399883256425,-72.4385039748556));
#68977=CARTESIAN_POINT('Ctrl Pts',(-22.8432624237119,27.4191870086807,-72.4443762832492));
#68978=CARTESIAN_POINT('Ctrl Pts',(-22.7295767608545,27.3984126483142,-72.4502409816707));
#68979=CARTESIAN_POINT('Ctrl Pts',(-22.6166515357721,27.3725946828935,-72.4561056800922));
#68980=CARTESIAN_POINT('Ctrl Pts',(-22.5049675148465,27.3418047512415,-72.4619703785137));
#68981=CARTESIAN_POINT('Ctrl Pts',(-22.3933983528712,27.3110464848107,-72.4678290455164));
#68982=CARTESIAN_POINT('Ctrl Pts',(-22.2830682521687,27.2753265319876,-72.4736877125191));
#68983=CARTESIAN_POINT('Ctrl Pts',(-22.1744483417286,27.2347676735918,-72.4795463795218));
#68984=CARTESIAN_POINT('Ctrl Pts',(-22.0615859437967,27.1926246631864,-72.4856338749352));
#68985=CARTESIAN_POINT('Ctrl Pts',(-21.9505705002284,27.1452571266615,-72.4917213703486));
#68986=CARTESIAN_POINT('Ctrl Pts',(-21.8419141592654,27.0928601878265,-72.497808865762));
#68987=CARTESIAN_POINT('Ctrl Pts',(-21.7374633129529,27.0424912488673,-72.5036607474122));
#68988=CARTESIAN_POINT('Ctrl Pts',(-21.635192755677,26.9874751867753,-72.5095126290623));
#68989=CARTESIAN_POINT('Ctrl Pts',(-21.5355368181626,26.9280342880617,-72.5153645107125));
#68990=CARTESIAN_POINT('Ctrl Pts',(-21.4358960542298,26.8686024398005,-72.521215501357));
#68991=CARTESIAN_POINT('Ctrl Pts',(-21.3388694734326,26.8047473061974,-72.5270664920015));
#68992=CARTESIAN_POINT('Ctrl Pts',(-21.2448653556963,26.7367363255875,-72.532917482646));
#68993=CARTESIAN_POINT('Ctrl Pts',(-21.1508527863816,26.6687192303504,-72.5387689993324));
#68994=CARTESIAN_POINT('Ctrl Pts',(-21.0598635552576,26.5965457876734,-72.5446205160188));
#68995=CARTESIAN_POINT('Ctrl Pts',(-20.972275002165,26.5205253907498,-72.5504720327052));
#68996=CARTESIAN_POINT('Ctrl Pts',(-20.884657363322,26.4444797495425,-72.5563254925194));
#68997=CARTESIAN_POINT('Ctrl Pts',(-20.8004429600238,26.364584884741,-72.5621789523336));
#68998=CARTESIAN_POINT('Ctrl Pts',(-20.7199737031995,26.2811884066232,-72.5680324121478));
#68999=CARTESIAN_POINT('Ctrl Pts',(-20.6394129369394,26.197697090241,-72.5738925285018));
#69000=CARTESIAN_POINT('Ctrl Pts',(-20.5626061051385,26.1106965101942,-72.5797526448558));
#69001=CARTESIAN_POINT('Ctrl Pts',(-20.4898561606954,26.0205689187948,-72.5856127612097));
#69002=CARTESIAN_POINT('Ctrl Pts',(-20.4170572243753,25.9303806329176,-72.5914768239323));
#69003=CARTESIAN_POINT('Ctrl Pts',(-20.3483208599742,25.8370614746095,-72.597340886655));
#69004=CARTESIAN_POINT('Ctrl Pts',(-20.2839068432094,25.7410229083692,-72.6032049493776));
#69005=CARTESIAN_POINT('Ctrl Pts',(-20.2193978949256,25.6448428032615,-72.6090776543866));
#69006=CARTESIAN_POINT('Ctrl Pts',(-20.159224221921,25.5459356432879,-72.6149503593956));
#69007=CARTESIAN_POINT('Ctrl Pts',(-20.1035998544535,25.4447377711377,-72.6208230644046));
#69008=CARTESIAN_POINT('Ctrl Pts',(-20.0883719070233,25.4170334403325,-72.6224307994176));
#69009=CARTESIAN_POINT('Ctrl Pts',(-20.0734846362955,25.389157542895,-72.6240385344305));
#69010=CARTESIAN_POINT('Ctrl Pts',(-20.0589417975363,25.3611192737694,-72.6256462694435));
#69011=CARTESIAN_POINT('Ctrl Pts',(-20.005823932946,25.2587092142599,-72.6315185377213));
#69012=CARTESIAN_POINT('Ctrl Pts',(-19.9571268640713,25.1537884528487,-72.6373908059991));
#69013=CARTESIAN_POINT('Ctrl Pts',(-19.913095915983,25.0467754191864,-72.6432630742769));
#69014=CARTESIAN_POINT('Ctrl Pts',(-19.8691220289086,24.9399010668942,-72.6491277325077));
#69015=CARTESIAN_POINT('Ctrl Pts',(-19.8298023932249,24.8309402131891,-72.6549923907386));
#69016=CARTESIAN_POINT('Ctrl Pts',(-19.7953366132564,24.720336052415,-72.6608570489695));
#69017=CARTESIAN_POINT('Ctrl Pts',(-19.7609062792614,24.6098456413412,-72.6667156757535));
#69018=CARTESIAN_POINT('Ctrl Pts',(-19.7313199940879,24.4977156770748,-72.6725743025375));
#69019=CARTESIAN_POINT('Ctrl Pts',(-19.7067291261628,24.3844088906175,-72.6784329293215));
#69020=CARTESIAN_POINT('Ctrl Pts',(-19.6811775469786,24.2666754566009,-72.6845204398005));
#69021=CARTESIAN_POINT('Ctrl Pts',(-19.6610198365035,24.1476717943016,-72.6906079502796));
#69022=CARTESIAN_POINT('Ctrl Pts',(-19.6463686755074,24.0279342640268,-72.6966954607586));
#69023=CARTESIAN_POINT('Ctrl Pts',(-19.6322847123097,23.9128321932603,-72.7025473023687));
#69024=CARTESIAN_POINT('Ctrl Pts',(-19.6232889269094,23.7970524675998,-72.7083991439788));
#69025=CARTESIAN_POINT('Ctrl Pts',(-19.6194290805156,23.6810806466566,-72.7142509855889));
#69026=CARTESIAN_POINT('Ctrl Pts',(-19.6155698217372,23.5651264810349,-72.7201019363261));
#69027=CARTESIAN_POINT('Ctrl Pts',(-19.6168449610749,23.4489806913225,-72.7259528870634));
#69028=CARTESIAN_POINT('Ctrl Pts',(-19.6232501911883,23.3331313266936,-72.7318038378006));
#69029=CARTESIAN_POINT('Ctrl Pts',(-19.6296559973681,23.2172715429345,-72.7376553147541));
#69030=CARTESIAN_POINT('Ctrl Pts',(-19.6411927886908,23.1017086500372,-72.7435067917076));
#69031=CARTESIAN_POINT('Ctrl Pts',(-19.6578042360617,22.9869273451213,-72.7493582686611));
#69032=CARTESIAN_POINT('Ctrl Pts',(-19.6744212002883,22.8721079199931,-72.7552116889584));
#69033=CARTESIAN_POINT('Ctrl Pts',(-19.6961161126017,22.7580710079023,-72.7610651092558));
#69034=CARTESIAN_POINT('Ctrl Pts',(-19.722781340422,22.6452921568815,-72.7669185295531));
#69035=CARTESIAN_POINT('Ctrl Pts',(-19.7494768944375,22.5323850431853,-72.7727786069084));
#69036=CARTESIAN_POINT('Ctrl Pts',(-19.7811539514199,22.4207392488964,-72.7786386842637));
#69037=CARTESIAN_POINT('Ctrl Pts',(-19.8176546754305,22.3108162713663,-72.784498761619));
#69038=CARTESIAN_POINT('Ctrl Pts',(-19.8541799818049,22.2008192633424,-72.7903627855961));
#69039=CARTESIAN_POINT('Ctrl Pts',(-19.8955352767182,22.0925477676481,-72.7962268095732));
#69040=CARTESIAN_POINT('Ctrl Pts',(-19.9415148085408,21.9864427461097,-72.8020908335503));
#69041=CARTESIAN_POINT('Ctrl Pts',(-19.987562109383,21.8801813368702,-72.8079635004853));
#69042=CARTESIAN_POINT('Ctrl Pts',(-20.0382470695384,21.7760931449798,-72.8138361674203));
#69043=CARTESIAN_POINT('Ctrl Pts',(-20.0933182797116,21.6745940933134,-72.8197088343552));
#69044=CARTESIAN_POINT('Ctrl Pts',(-20.1083984582723,21.6468005544015,-72.821316949843));
#69045=CARTESIAN_POINT('Ctrl Pts',(-20.1238072844074,21.6192009847867,-72.8229250653307));
#69046=CARTESIAN_POINT('Ctrl Pts',(-20.1395390479644,21.5918035198729,-72.8245331808184));
#69047=CARTESIAN_POINT('Ctrl Pts',(-20.1969863325208,21.4917568876362,-72.8304054956219));
#69048=CARTESIAN_POINT('Ctrl Pts',(-20.2589355974952,21.3940724510578,-72.8362778104255));
#69049=CARTESIAN_POINT('Ctrl Pts',(-20.3251674142848,21.299182789224,-72.8421501252291));
#69050=CARTESIAN_POINT('Ctrl Pts',(-20.3913133981876,21.2044160993093,-72.8480148298272));
#69051=CARTESIAN_POINT('Ctrl Pts',(-20.4617306626143,21.1124373173681,-72.8538795344253));
#69052=CARTESIAN_POINT('Ctrl Pts',(-20.5361542301702,21.0236539429291,-72.8597442390235));
#69053=CARTESIAN_POINT('Ctrl Pts',(-20.610501255532,20.9349618792737,-72.8656029119656));
#69054=CARTESIAN_POINT('Ctrl Pts',(-20.6888461244686,20.8494590012516,-72.8714615849077));
#69055=CARTESIAN_POINT('Ctrl Pts',(-20.7708813496616,20.7675227869136,-72.8773202578498));
#69056=CARTESIAN_POINT('Ctrl Pts',(-20.8561205961699,20.682386418293,-72.8834077509475));
#69057=CARTESIAN_POINT('Ctrl Pts',(-20.945344080629,20.6011013691313,-72.8894952440452));
#69058=CARTESIAN_POINT('Ctrl Pts',(-21.038161470082,20.5240523568597,-72.8955827371428));
#69059=CARTESIAN_POINT('Ctrl Pts',(-21.1273865193826,20.4499853963579,-72.9014346241109));
#69060=CARTESIAN_POINT('Ctrl Pts',(-21.219932106138,20.3798329604736,-72.907286511079));
#69061=CARTESIAN_POINT('Ctrl Pts',(-21.3154155334049,20.3138977008579,-72.9131383980471));
#69062=CARTESIAN_POINT('Ctrl Pts',(-21.4108844185471,20.2479724831814,-72.9189893937729));
#69063=CARTESIAN_POINT('Ctrl Pts',(-21.5092899144949,20.1862633995526,-72.9248403894987));
#69064=CARTESIAN_POINT('Ctrl Pts',(-21.6102190844596,20.1290306412563,-72.9306913852245));
#69065=CARTESIAN_POINT('Ctrl Pts',(-21.7111573244478,20.0717927397249,-72.9365429067514));
#69066=CARTESIAN_POINT('Ctrl Pts',(-21.8146193296805,20.0190321671141,-72.9423944282783));
#69067=CARTESIAN_POINT('Ctrl Pts',(-21.9201668633793,19.9709635361038,-72.9482459498052));
#69068=CARTESIAN_POINT('Ctrl Pts',(-22.025749442061,19.9228789448499,-72.9540994142148));
#69069=CARTESIAN_POINT('Ctrl Pts',(-22.133418550115,19.8794895641573,-72.9599528786243));
#69070=CARTESIAN_POINT('Ctrl Pts',(-22.2427159160716,19.8409618988634,-72.9658063430339));
#69071=CARTESIAN_POINT('Ctrl Pts',(-22.3521375674535,19.8023904225662,-72.9716664635994));
#69072=CARTESIAN_POINT('Ctrl Pts',(-22.4631907822626,19.7686918337133,-72.9775265841649));
#69073=CARTESIAN_POINT('Ctrl Pts',(-22.575401972787,19.7399828053102,-72.9833867047304));
#69074=CARTESIAN_POINT('Ctrl Pts',(-22.6876887252861,19.7112544445137,-72.9892507714467));
#69075=CARTESIAN_POINT('Ctrl Pts',(-22.8011346025448,19.6875224188809,-72.9951148381631));
#69076=CARTESIAN_POINT('Ctrl Pts',(-22.9152573927853,19.6688519889053,-73.0009789048794));
#69077=CARTESIAN_POINT('Ctrl Pts',(-23.0295483670025,19.6501540441173,-73.0068516135336));
#69078=CARTESIAN_POINT('Ctrl Pts',(-23.1445178361985,19.6365326308205,-73.0127243221878));
#69079=CARTESIAN_POINT('Ctrl Pts',(-23.2596799739163,19.6280010623636,-73.0185970308419));
#69080=CARTESIAN_POINT('Ctrl Pts',(-23.2912062586497,19.625665497379,-73.020204717959));
#69081=CARTESIAN_POINT('Ctrl Pts',(-23.3227469939116,19.6237110750981,-73.0218124050761));
#69082=CARTESIAN_POINT('Ctrl Pts',(-23.3542922566749,19.6221373894645,-73.0234200921933));
#69083=CARTESIAN_POINT('Ctrl Pts',(-23.4695169340422,19.616389223067,-73.0292924550506));
#69084=CARTESIAN_POINT('Ctrl Pts',(-23.5851877451827,19.6157056112334,-73.035164817908));
#69085=CARTESIAN_POINT('Ctrl Pts',(-23.7008221353131,19.6201357656851,-73.0410371807653));
#69086=CARTESIAN_POINT('Ctrl Pts',(-23.8163066823252,19.6245601793865,-73.0469019340079));
#69087=CARTESIAN_POINT('Ctrl Pts',(-23.9317544929248,19.6340851657604,-73.0527666872505));
#69088=CARTESIAN_POINT('Ctrl Pts',(-24.0466794920465,19.6487080589199,-73.0586314404931));
#69089=CARTESIAN_POINT('Ctrl Pts',(-24.1614863058885,19.6633159143528,-73.0644901626067));
#69090=CARTESIAN_POINT('Ctrl Pts',(-24.2757709700512,19.6830111970448,-73.0703488847202));
#69091=CARTESIAN_POINT('Ctrl Pts',(-24.3890496894398,19.707739248938,-73.0762076068337));
#69092=CARTESIAN_POINT('Ctrl Pts',(-24.5067513560378,19.7334328031665,-73.0822950816976));
#69093=CARTESIAN_POINT('Ctrl Pts',(-24.6233664689073,19.7645601250094,-73.0883825565616));
#69094=CARTESIAN_POINT('Ctrl Pts',(-24.7383603790814,19.8010007739461,-73.0944700314255));
#69095=CARTESIAN_POINT('Ctrl Pts',(-24.848904923149,19.8360314544069,-73.1003219685615));
#69096=CARTESIAN_POINT('Ctrl Pts',(-24.9579509576739,19.8759717992191,-73.1061739056974));
#69097=CARTESIAN_POINT('Ctrl Pts',(-25.0650369873523,19.9206634292066,-73.1120258428334));
#69098=CARTESIAN_POINT('Ctrl Pts',(-25.1721067131054,19.9653482548612,-73.1178768890077));
#69099=CARTESIAN_POINT('Ctrl Pts',(-25.2772166459731,20.0147827682002,-73.123727935182));
#69100=CARTESIAN_POINT('Ctrl Pts',(-25.3799246677479,20.0687601972852,-73.1295789813563));
#69101=CARTESIAN_POINT('Ctrl Pts',(-25.4826419232885,20.1227424791064,-73.1354305535576));
#69102=CARTESIAN_POINT('Ctrl Pts',(-25.5829564725298,20.1812682962628,-73.1412821257589));
#69103=CARTESIAN_POINT('Ctrl Pts',(-25.6804508678707,20.2440849544908,-73.1471336979602));
#69104=CARTESIAN_POINT('Ctrl Pts',(-25.7779776368804,20.3069224714121,-73.1529872132153));
#69105=CARTESIAN_POINT('Ctrl Pts',(-25.8726820426087,20.3740534387639,-73.1588407284705));
#69106=CARTESIAN_POINT('Ctrl Pts',(-25.9641762819582,20.445182302551,-73.1646942437256));
#69107=CARTESIAN_POINT('Ctrl Pts',(-26.0557745612392,20.5163920483933,-73.1705544151301));
#69108=CARTESIAN_POINT('Ctrl Pts',(-26.1441550616155,20.5916085106643,-73.1764145865347));
#69109=CARTESIAN_POINT('Ctrl Pts',(-26.2289636253595,20.6704963134225,-73.1822747579392));
#69110=CARTESIAN_POINT('Ctrl Pts',(-26.3138292987582,20.7494372388252,-73.1881388755533));
#69111=CARTESIAN_POINT('Ctrl Pts',(-26.3951179568315,20.8320541335458,-73.1940029931674));
#69112=CARTESIAN_POINT('Ctrl Pts',(-26.4725140343758,20.9179765754265,-73.1998671107815));
#69113=CARTESIAN_POINT('Ctrl Pts',(-26.5500241662413,21.0040256364601,-73.2057398700216));
#69114=CARTESIAN_POINT('Ctrl Pts',(-26.6236300072429,21.0933896487596,-73.2116126292616));
#69115=CARTESIAN_POINT('Ctrl Pts',(-26.6930577422606,21.1856670694119,-73.2174853885017));
#69116=CARTESIAN_POINT('Ctrl Pts',(-26.7120581132677,21.2109207411257,-73.2190925935239));
#69117=CARTESIAN_POINT('Ctrl Pts',(-26.7307458206822,21.236392462215,-73.220699798546));
#69118=CARTESIAN_POINT('Ctrl Pts',(-26.7491158468198,21.2620736726136,-73.2223070035682));
#69119=CARTESIAN_POINT('Ctrl Pts',(-26.8168479191964,21.3567627921826,-73.2282329247437));
#69120=CARTESIAN_POINT('Ctrl Pts',(-26.8804833326209,21.4546172015587,-73.2341588459192));
#69121=CARTESIAN_POINT('Ctrl Pts',(-26.9397153837474,21.5552511345641,-73.2400847670947));
#69122=CARTESIAN_POINT('Ctrl Pts',(-26.9988677778658,21.6557497320901,-73.2460027189167));
#69123=CARTESIAN_POINT('Ctrl Pts',(-27.0536283845837,21.7590200748152,-73.2519206707387));
#69124=CARTESIAN_POINT('Ctrl Pts',(-27.1037321446487,21.8646453294325,-73.2578386225608));
#69125=CARTESIAN_POINT('Ctrl Pts',(-27.1537799057791,21.970152530999,-73.2637499601288));
#69126=CARTESIAN_POINT('Ctrl Pts',(-27.1991810022792,22.0780090466331,-73.2696612976968));
#69127=CARTESIAN_POINT('Ctrl Pts',(-27.2397152263503,22.1877716970617,-73.2755726352648));
#69128=CARTESIAN_POINT('Ctrl Pts',(-27.2802088669413,22.2974244514591,-73.2814780543119));
#69129=CARTESIAN_POINT('Ctrl Pts',(-27.3158451972843,22.4089791642609,-73.287383473359));
#69130=CARTESIAN_POINT('Ctrl Pts',(-27.3464515726025,22.5219715186406,-73.2932888924061));
#69131=CARTESIAN_POINT('Ctrl Pts',(-27.3770395349175,22.6348958960523,-73.299190758713));
#69132=CARTESIAN_POINT('Ctrl Pts',(-27.4026034574628,22.7492558059355,-73.30509262502));
#69133=CARTESIAN_POINT('Ctrl Pts',(-27.423020232726,22.8645708753517,-73.3109944913269));
#69134=CARTESIAN_POINT('Ctrl Pts',(-27.4434322422425,22.9798590275683,-73.3168949800019));
#69135=CARTESIAN_POINT('Ctrl Pts',(-27.4586994176279,23.0961015000886,-73.3227954686769));
#69136=CARTESIAN_POINT('Ctrl Pts',(-27.468749644824,23.2128071666449,-73.328695957352));
#69137=CARTESIAN_POINT('Ctrl Pts',(-27.4784813882952,23.3258145232347,-73.334409464223));
#69138=CARTESIAN_POINT('Ctrl Pts',(-27.4833218019471,23.4392557983426,-73.340122971094));
#69139=CARTESIAN_POINT('Ctrl Pts',(-27.4832517822853,23.5526804628563,-73.345836477965));
#69140=CARTESIAN_POINT('Ctrl Pts',(-27.4782612161635,23.552707293754,-73.3458379866115));
#69141=CARTESIAN_POINT('Ctrl Pts',(-27.4810432214932,24.0507322526134,-73.3709566293887));
#69142=CARTESIAN_POINT('Ctrl Pts',(-27.1616604773278,25.8597480102053,-73.4623709092908));
#69143=CARTESIAN_POINT('Ctrl Pts',(-24.4392995286466,28.1164329704807,-73.620080826318));
#69144=CARTESIAN_POINT('Ctrl Pts',(-20.1891690511146,26.7665256923699,-73.8189677376927));
#69145=CARTESIAN_POINT('Ctrl Pts',(-19.0276283246582,22.4608807262844,-74.0178546490677));
#69146=CARTESIAN_POINT('Ctrl Pts',(-22.0219221388387,19.1567582508198,-74.2167415604425));
#69147=CARTESIAN_POINT('Ctrl Pts',(-26.2830391088016,19.8660492331889,-74.4094015795675));
#69148=CARTESIAN_POINT('Ctrl Pts',(-27.4805056762975,22.3695229369242,-74.5357659615675));
#69149=CARTESIAN_POINT('Ctrl Pts',(-27.4882738925428,23.5526426182486,-74.5958347064426));
#69150=CARTESIAN_POINT('Origin',(-23.5502525316942,23.5502525316942,-77.3107734492734));
#69151=CARTESIAN_POINT('',(-21.7179950055095,20.8990358449182,30.));
#69152=CARTESIAN_POINT('Ctrl Pts',(-21.7179950055095,20.8990358449182,30.));
#69153=CARTESIAN_POINT('Ctrl Pts',(-21.9298629608487,20.7526137672118,29.9831668988443));
#69154=CARTESIAN_POINT('Ctrl Pts',(-22.1585744966718,20.6320761596675,29.9653743087997));
#69155=CARTESIAN_POINT('Ctrl Pts',(-22.5126273183095,20.4967004425218,29.9400899248691));
#69156=CARTESIAN_POINT('Ctrl Pts',(-22.628353293357,20.459790786396,29.9321326957846));
#69157=CARTESIAN_POINT('Ctrl Pts',(-22.8159383538087,20.4114419441816,29.9197544699574));
#69158=CARTESIAN_POINT('Ctrl Pts',(-22.8865714104851,20.3957513134557,29.9152061722286));
#69159=CARTESIAN_POINT('Ctrl Pts',(-22.9662854811856,20.3808398517232,29.910191053069));
#69160=CARTESIAN_POINT('Ctrl Pts',(-22.9749000208742,20.3792647135659,29.9096506001298));
#69161=CARTESIAN_POINT('Ctrl Pts',(-22.9877931533489,20.3769615200717,29.9088439626519));
#69162=CARTESIAN_POINT('Ctrl Pts',(-22.9920669189485,20.3762069714118,29.908576949571));
#69163=CARTESIAN_POINT('Ctrl Pts',(-22.9993978136246,20.3749279399407,29.9081195617715));
#69164=CARTESIAN_POINT('Ctrl Pts',(-23.0024541910024,20.3743992351063,29.9079290553469));
#69165=CARTESIAN_POINT('Ctrl Pts',(-23.008730027137,20.3733229441465,29.9075382582219));
#69166=CARTESIAN_POINT('Ctrl Pts',(-23.0119495648089,20.3727758373445,29.9073379827214));
#69167=CARTESIAN_POINT('Ctrl Pts',(-23.0196698025262,20.3714759820123,29.9068582250794));
#69168=CARTESIAN_POINT('Ctrl Pts',(-23.024171289719,20.3707278954502,29.9065788885492));
#69169=CARTESIAN_POINT('Ctrl Pts',(-23.037887446517,20.3684783810228,29.90572894625));
#69170=CARTESIAN_POINT('Ctrl Pts',(-23.0471071202861,20.3670074226602,29.9051592892992));
#69171=CARTESIAN_POINT('Ctrl Pts',(-23.1489625406978,20.3512104096274,29.8988838468123));
#69172=CARTESIAN_POINT('Ctrl Pts',(-23.242180281236,20.3408915091698,29.8933059483484));
#69173=CARTESIAN_POINT('Ctrl Pts',(-23.4963027679233,20.3239376477752,29.8784264564005));
#69174=CARTESIAN_POINT('Ctrl Pts',(-23.657468210975,20.3252674899317,29.8693523304162));
#69175=CARTESIAN_POINT('Ctrl Pts',(-23.9685073654848,20.3511853595039,29.8518110266293));
#69176=CARTESIAN_POINT('Ctrl Pts',(-24.1180692247852,20.3743201719093,29.8433583321896));
#69177=CARTESIAN_POINT('Ctrl Pts',(-24.3429114255277,20.4254931187756,29.8299590348898));
#69178=CARTESIAN_POINT('Ctrl Pts',(-24.4196929418666,20.4459811791637,29.825254310171));
#69179=CARTESIAN_POINT('Ctrl Pts',(-24.5042521220368,20.471927719796,29.8198491575605));
#69180=CARTESIAN_POINT('Ctrl Pts',(-24.5128610275461,20.4746089006265,29.8192962413981));
#69181=CARTESIAN_POINT('Ctrl Pts',(-24.5277058470465,20.4793006422308,29.8183381027039));
#69182=CARTESIAN_POINT('Ctrl Pts',(-24.5339471418504,20.4812941736653,29.8179338232026));
#69183=CARTESIAN_POINT('Ctrl Pts',(-24.5427974175166,20.4841508106583,29.8173584387305));
#69184=CARTESIAN_POINT('Ctrl Pts',(-24.5454114917559,20.4849982586869,29.8171882279141));
#69185=CARTESIAN_POINT('Ctrl Pts',(-24.5497496339647,20.4864107608489,29.8169053180814));
#69186=CARTESIAN_POINT('Ctrl Pts',(-24.5514743207105,20.4869739313406,29.8167927280635));
#69187=CARTESIAN_POINT('Ctrl Pts',(-24.555053082414,20.4881458673242,29.8165588599876));
#69188=CARTESIAN_POINT('Ctrl Pts',(-24.5569070810166,20.4887548607843,29.8164375686648));
#69189=CARTESIAN_POINT('Ctrl Pts',(-24.5613881423805,20.4902312910431,29.8161440829554));
#69190=CARTESIAN_POINT('Ctrl Pts',(-24.5640146348641,20.4911004245828,29.8159717886689));
#69191=CARTESIAN_POINT('Ctrl Pts',(-24.5729614638971,20.4940738102851,29.8153839660973));
#69192=CARTESIAN_POINT('Ctrl Pts',(-24.579276341819,20.4961942589145,29.8149674966045));
#69193=CARTESIAN_POINT('Ctrl Pts',(-24.6842763549335,20.5318144373344,29.808017049784));
#69194=CARTESIAN_POINT('Ctrl Pts',(-24.7812749973739,20.5700583880627,29.8012202361129));
#69195=CARTESIAN_POINT('Ctrl Pts',(-24.9538128011945,20.6479465189471,29.788642057707));
#69196=CARTESIAN_POINT('Ctrl Pts',(-25.0299664674638,20.6860236182878,29.7829071454149));
#69197=CARTESIAN_POINT('Ctrl Pts',(-25.2441722546298,20.8039519091449,29.7663844271414));
#69198=CARTESIAN_POINT('Ctrl Pts',(-25.3779362146065,20.8910966595255,29.7555900994215));
#69199=CARTESIAN_POINT('Ctrl Pts',(-25.5816319379943,21.0464603735282,29.7386684696809));
#69200=CARTESIAN_POINT('Ctrl Pts',(-25.6558812309435,21.1085711046002,29.7323797290813));
#69201=CARTESIAN_POINT('Ctrl Pts',(-25.7738526902579,21.2166463129568,29.7221948715367));
#69202=CARTESIAN_POINT('Ctrl Pts',(-25.8192114163984,21.2607237288694,29.7182264821787));
#69203=CARTESIAN_POINT('Ctrl Pts',(-25.869111756015,21.3121550350113,29.7137950129729));
#69204=CARTESIAN_POINT('Ctrl Pts',(-25.8749532783229,21.3182231977364,29.7132751809532));
#69205=CARTESIAN_POINT('Ctrl Pts',(-25.8836989401452,21.3273797526832,29.7124952759405));
#69206=CARTESIAN_POINT('Ctrl Pts',(-25.8866208517964,21.3304510527603,29.7122344340904));
#69207=CARTESIAN_POINT('Ctrl Pts',(-25.8916383313928,21.3357459421734,29.7117860376474));
#69208=CARTESIAN_POINT('Ctrl Pts',(-25.89373680711,21.3379667569721,29.7115983578546));
#69209=CARTESIAN_POINT('Ctrl Pts',(-25.8980544223111,21.3425491217386,29.7112119042922));
#69210=CARTESIAN_POINT('Ctrl Pts',(-25.9002731648341,21.3449110416195,29.7110131477093));
#69211=CARTESIAN_POINT('Ctrl Pts',(-25.9056100235284,21.3506094917643,29.7105346666166));
#69212=CARTESIAN_POINT('Ctrl Pts',(-25.9087246241701,21.3539493179254,29.7102550927863));
#69213=CARTESIAN_POINT('Ctrl Pts',(-25.9182743178774,21.3642333153892,29.7093968596217));
#69214=CARTESIAN_POINT('Ctrl Pts',(-25.9246859591711,21.3711992750332,29.7088191998655));
#69215=CARTESIAN_POINT('Ctrl Pts',(-25.9999572425682,21.4537048346496,29.7020201299799));
#69216=CARTESIAN_POINT('Ctrl Pts',(-26.0652208138656,21.5324558916646,29.6959543552564));
#69217=CARTESIAN_POINT('Ctrl Pts',(-26.1283647047898,21.6164832940963,29.6898427359488));
#69218=CARTESIAN_POINT('Ctrl Pts',(-26.1300901657968,21.6187858291399,29.6896755296771));
#69219=CARTESIAN_POINT('Ctrl Pts',(-26.2775093540809,21.8160587953789,29.6753724565649));
#69220=CARTESIAN_POINT('Ctrl Pts',(-26.4006468986361,22.0268970767938,29.6620447908319));
#69221=CARTESIAN_POINT('Ctrl Pts',(-26.5374445743441,22.3370203294724,29.6429444056442));
#69222=CARTESIAN_POINT('Ctrl Pts',(-26.5721000086692,22.4261155195152,29.6375000200887));
#69223=CARTESIAN_POINT('Ctrl Pts',(-26.6227336822201,22.5756441265718,29.6282375515535));
#69224=CARTESIAN_POINT('Ctrl Pts',(-26.641005119485,22.6352393168289,29.6245139306103));
#69225=CARTESIAN_POINT('Ctrl Pts',(-26.6602931856184,22.7053426477049,29.6200565536783));
#69226=CARTESIAN_POINT('Ctrl Pts',(-26.6630017569354,22.7153765918689,29.6194167394031));
#69227=CARTESIAN_POINT('Ctrl Pts',(-26.6664892658084,22.7285490361741,29.6185741966033));
#69228=CARTESIAN_POINT('Ctrl Pts',(-26.6673121204535,22.7316760004533,29.6183739962105));
#69229=CARTESIAN_POINT('Ctrl Pts',(-26.668637508965,22.7367436412484,29.6180492276507));
#69230=CARTESIAN_POINT('Ctrl Pts',(-26.6691429429946,22.7386835675589,29.6179248285545));
#69231=CARTESIAN_POINT('Ctrl Pts',(-26.6701092461706,22.742406608542,29.6176859388827));
#69232=CARTESIAN_POINT('Ctrl Pts',(-26.6705703955044,22.7441896413548,29.6175714653879));
#69233=CARTESIAN_POINT('Ctrl Pts',(-26.6716269330408,22.7482892345219,29.6173081150987));
#69234=CARTESIAN_POINT('Ctrl Pts',(-26.6722212667572,22.7506060469319,29.617159177712));
#69235=CARTESIAN_POINT('Ctrl Pts',(-26.6740222972519,22.7576593793744,29.6167054219028));
#69236=CARTESIAN_POINT('Ctrl Pts',(-26.6752207909294,22.7623979567029,29.616400127919));
#69237=CARTESIAN_POINT('Ctrl Pts',(-26.6843034179204,22.7986554273766,29.6140608048123));
#69238=CARTESIAN_POINT('Ctrl Pts',(-26.6917209266959,22.830287750922,29.612000558304));
#69239=CARTESIAN_POINT('Ctrl Pts',(-26.7374078438757,23.0392898786938,29.5982856506814));
#69240=CARTESIAN_POINT('Ctrl Pts',(-26.761113384066,23.2194933337451,29.5859957193082));
#69241=CARTESIAN_POINT('Ctrl Pts',(-26.7787621559303,23.5994356026406,29.5602348194704));
#69242=CARTESIAN_POINT('Ctrl Pts',(-26.7695740247474,23.7986108341445,29.5468310377809));
#69243=CARTESIAN_POINT('Ctrl Pts',(-26.734137425529,24.0525367763684,29.5302452816274));
#69244=CARTESIAN_POINT('Ctrl Pts',(-26.7246858508568,24.1091677791813,29.5265760112754));
#69245=CARTESIAN_POINT('Ctrl Pts',(-26.7052298986207,24.2092031009733,29.5201461968322));
#69246=CARTESIAN_POINT('Ctrl Pts',(-26.6958295123921,24.2527080960775,29.5173674241366));
#69247=CARTESIAN_POINT('Ctrl Pts',(-26.6837606698719,24.3034476038151,29.5141451243775));
#69248=CARTESIAN_POINT('Ctrl Pts',(-26.6819641855773,24.3108826568239,29.5136734155555));
#69249=CARTESIAN_POINT('Ctrl Pts',(-26.6791771645141,24.3222399463337,29.5129535599061));
#69250=CARTESIAN_POINT('Ctrl Pts',(-26.6782056940745,24.3261667926946,29.5127047930568));
#69251=CARTESIAN_POINT('Ctrl Pts',(-26.6764238668061,24.3333115059672,29.5122524015377));
#69252=CARTESIAN_POINT('Ctrl Pts',(-26.6756159299215,24.3365299654396,29.5120486983328));
#69253=CARTESIAN_POINT('Ctrl Pts',(-26.6739843471008,24.3429872136368,29.5116401723345));
#69254=CARTESIAN_POINT('Ctrl Pts',(-26.6731606314016,24.346225980658,29.5114353520998));
#69255=CARTESIAN_POINT('Ctrl Pts',(-26.670810230119,24.3554077109653,29.5108549339681));
#69256=CARTESIAN_POINT('Ctrl Pts',(-26.6692716019104,24.3613476262194,29.510479726348));
#69257=CARTESIAN_POINT('Ctrl Pts',(-26.6627322324901,24.3862992559835,29.508904751374));
#69258=CARTESIAN_POINT('Ctrl Pts',(-26.6575744813119,24.405269690207,29.5077101267986));
#69259=CARTESIAN_POINT('Ctrl Pts',(-26.5464090093256,24.7998442096166,29.4829153174042));
#69260=CARTESIAN_POINT('Ctrl Pts',(-26.3732515597564,25.1530847453112,29.4622281856888));
#69261=CARTESIAN_POINT('Ctrl Pts',(-26.0938334325533,25.5308215645426,29.4352713542118));
#69262=CARTESIAN_POINT('Ctrl Pts',(-26.0441292729003,25.5930531111164,29.4306229963969));
#69263=CARTESIAN_POINT('Ctrl Pts',(-25.9715330284493,25.6773442045163,29.4239293092894));
#69264=CARTESIAN_POINT('Ctrl Pts',(-25.9505387300426,25.7010068666755,29.4220038356843));
#69265=CARTESIAN_POINT('Ctrl Pts',(-25.9261417111635,25.7277025835267,29.4197726191509));
#69266=CARTESIAN_POINT('Ctrl Pts',(-25.9230758609738,25.7310431151222,29.4194923454347));
#69267=CARTESIAN_POINT('Ctrl Pts',(-25.9184602189465,25.7360510344415,29.4190705405192));
#69268=CARTESIAN_POINT('Ctrl Pts',(-25.9169156766902,25.7377232863818,29.4189294157396));
#69269=CARTESIAN_POINT('Ctrl Pts',(-25.9141315261297,25.7407312425984,29.418675069353));
#69270=CARTESIAN_POINT('Ctrl Pts',(-25.9128925546058,25.7420675342282,29.4185618975494));
#69271=CARTESIAN_POINT('Ctrl Pts',(-25.9102477594258,25.744915227483,29.4183203454948));
#69272=CARTESIAN_POINT('Ctrl Pts',(-25.9088416153029,25.7464263312435,29.4181919402884));
#69273=CARTESIAN_POINT('Ctrl Pts',(-25.9051152991176,25.7504230866298,29.4178517174421));
#69274=CARTESIAN_POINT('Ctrl Pts',(-25.9027926512932,25.7529064104562,29.4176397087285));
#69275=CARTESIAN_POINT('Ctrl Pts',(-25.8927703168508,25.7635881339019,29.4167251378481));
#69276=CARTESIAN_POINT('Ctrl Pts',(-25.8850317935019,25.7717497411225,29.4160196231809));
#69277=CARTESIAN_POINT('Ctrl Pts',(-25.7439877023938,25.9189540435713,29.4031752896231));
#69278=CARTESIAN_POINT('Ctrl Pts',(-25.5985400038457,26.0457926234618,29.3901856923264));
#69279=CARTESIAN_POINT('Ctrl Pts',(-25.284738071636,26.2734388172624,29.3639477691765));
#69280=CARTESIAN_POINT('Ctrl Pts',(-25.1167166413429,26.3734404623235,29.3507596549073));
#69281=CARTESIAN_POINT('Ctrl Pts',(-24.8691366058195,26.4918420723846,29.3328907835062));
#69282=CARTESIAN_POINT('Ctrl Pts',(-24.7963645604632,26.5234008258716,29.3278086661774));
#69283=CARTESIAN_POINT('Ctrl Pts',(-24.6850391244419,26.5668721624575,29.3202846481387));
#69284=CARTESIAN_POINT('Ctrl Pts',(-24.6473093960438,26.5807972154086,29.3177765632291));
#69285=CARTESIAN_POINT('Ctrl Pts',(-24.6022491107101,26.5964759197372,29.3148289069903));
#69286=CARTESIAN_POINT('Ctrl Pts',(-24.5951621016848,26.5989141600452,29.3143666899971));
#69287=CARTESIAN_POINT('Ctrl Pts',(-24.5842436404484,26.602628041936,29.3136566954193));
#69288=CARTESIAN_POINT('Ctrl Pts',(-24.5804182230257,26.6039212296944,29.3134083378077));
#69289=CARTESIAN_POINT('Ctrl Pts',(-24.5734430567413,26.6062645957357,29.3129562096452));
#69290=CARTESIAN_POINT('Ctrl Pts',(-24.5702941008127,26.6073171014268,29.3127523624552));
#69291=CARTESIAN_POINT('Ctrl Pts',(-24.5639168131349,26.6094376927881,29.3123400678684));
#69292=CARTESIAN_POINT('Ctrl Pts',(-24.560688405787,26.6105055391778,29.3121316285793));
#69293=CARTESIAN_POINT('Ctrl Pts',(-24.5514601976808,26.6135417187981,29.311536609632));
#69294=CARTESIAN_POINT('Ctrl Pts',(-24.5454562705332,26.6154975387618,29.3111504424672));
#69295=CARTESIAN_POINT('Ctrl Pts',(-24.5196478806968,26.6238209758197,29.3094945332828));
#69296=CARTESIAN_POINT('Ctrl Pts',(-24.4997874516919,26.6300145014779,29.3082305186263));
#69297=CARTESIAN_POINT('Ctrl Pts',(-24.1430899814698,26.737473022109,29.2857055377371));
#69298=CARTESIAN_POINT('Ctrl Pts',(-23.7920122253475,26.7831121845741,29.2666957835297));
#69299=CARTESIAN_POINT('Ctrl Pts',(-23.3608145853837,26.7684175824128,29.2422175577395));
#69300=CARTESIAN_POINT('Ctrl Pts',(-23.2812726767628,26.7627470871028,29.2376389056326));
#69301=CARTESIAN_POINT('Ctrl Pts',(-23.145452268188,26.7479850030291,29.2295929228964));
#69302=CARTESIAN_POINT('Ctrl Pts',(-23.0890532080488,26.7403388081765,29.2261837029241));
#69303=CARTESIAN_POINT('Ctrl Pts',(-23.0231748368864,26.7296240976667,29.2220903805206));
#69304=CARTESIAN_POINT('Ctrl Pts',(-23.013466750109,26.7279994488734,29.2214843259563));
#69305=CARTESIAN_POINT('Ctrl Pts',(-23.0006365140691,26.7257918373753,29.2206794125919));
#69306=CARTESIAN_POINT('Ctrl Pts',(-22.9975074346999,26.725248674416,29.2204827965758));
#69307=CARTESIAN_POINT('Ctrl Pts',(-22.9924120988614,26.7243564370587,29.2201621162081));
#69308=CARTESIAN_POINT('Ctrl Pts',(-22.9904453454084,26.7240101570783,29.2200382115792));
#69309=CARTESIAN_POINT('Ctrl Pts',(-22.9866502114488,26.7233383225442,29.219798876431));
#69310=CARTESIAN_POINT('Ctrl Pts',(-22.9848217963528,26.7230130166587,29.2196834605371));
#69311=CARTESIAN_POINT('Ctrl Pts',(-22.9805850507495,26.7222554494987,29.2194157695822));
#69312=CARTESIAN_POINT('Ctrl Pts',(-22.9781769379555,26.7218220271269,29.2192634282119));
#69313=CARTESIAN_POINT('Ctrl Pts',(-22.9707491959713,26.7204764157812,29.2187929575582));
#69314=CARTESIAN_POINT('Ctrl Pts',(-22.9657312688389,26.7195550549269,29.2184743078043));
#69315=CARTESIAN_POINT('Ctrl Pts',(-22.9244925907579,26.7118817939853,29.2158489660614));
#69316=CARTESIAN_POINT('Ctrl Pts',(-22.888389731073,26.7045214549152,29.2135087623178));
#69317=CARTESIAN_POINT('Ctrl Pts',(-22.844730689279,26.6948381282827,29.2106343371644));
#69318=CARTESIAN_POINT('Ctrl Pts',(-22.8370447730954,26.6931038382261,29.2101266303812));
#69319=CARTESIAN_POINT('Ctrl Pts',(-22.8256244546952,26.6904828487402,29.2093698145893));
#69320=CARTESIAN_POINT('Ctrl Pts',(-22.8218850916567,26.6896176213396,29.2091216223243));
#69321=CARTESIAN_POINT('Ctrl Pts',(-22.5605843704022,26.6286649241888,29.191751648993));
#69322=CARTESIAN_POINT('Ctrl Pts',(-22.3114045873123,26.5371106962531,29.1734720195285));
#69323=CARTESIAN_POINT('Ctrl Pts',(-22.075820670606,26.4159406592144,29.1557691003147));
#69324=CARTESIAN_POINT('Ctrl Pts',(-22.0754283214049,26.4157387567432,29.1557396157498));
#69325=CARTESIAN_POINT('Ctrl Pts',(-22.0750360153802,26.4155367745738,29.1557101328919));
#69326=CARTESIAN_POINT('',(-25.421839063434,20.9266516823442,30.));
#69327=CARTESIAN_POINT('Origin',(-23.5502525316942,23.5502525316942,30.));
#69328=CARTESIAN_POINT('',(-26.7730025235471,23.5504816865032,29.8107734493065));
#69329=CARTESIAN_POINT('Ctrl Pts',(-26.7730025235471,23.5504816865032,29.8107734493065));
#69330=CARTESIAN_POINT('Ctrl Pts',(-26.7730097124841,23.4493790882664,29.8170642445203));
#69331=CARTESIAN_POINT('Ctrl Pts',(-26.7682549907641,23.3481129961194,29.8233550397341));
#69332=CARTESIAN_POINT('Ctrl Pts',(-26.7587181907666,23.2471590196342,29.8296458349478));
#69333=CARTESIAN_POINT('Ctrl Pts',(-26.7491960906962,23.1463606525867,29.8359269335934));
#69334=CARTESIAN_POINT('Ctrl Pts',(-26.7349066139694,23.0458738538775,29.8422080322391));
#69335=CARTESIAN_POINT('Ctrl Pts',(-26.7158815845527,22.9461745051131,29.8484891308848));
#69336=CARTESIAN_POINT('Ctrl Pts',(-26.6967600707826,22.8459695367783,29.8548020837646));
#69337=CARTESIAN_POINT('Ctrl Pts',(-26.6728548173153,22.7465604534429,29.8611150366444));
#69338=CARTESIAN_POINT('Ctrl Pts',(-26.6442511577937,22.6484265705495,29.8674279895242));
#69339=CARTESIAN_POINT('Ctrl Pts',(-26.6158621770808,22.5510292110741,29.873693561851));
#69340=CARTESIAN_POINT('Ctrl Pts',(-26.5828451813618,22.454888383564,29.8799591341779));
#69341=CARTESIAN_POINT('Ctrl Pts',(-26.5453347984475,22.3604627276196,29.8862247065047));
#69342=CARTESIAN_POINT('Ctrl Pts',(-26.5078496538264,22.266100604548,29.8924860631362));
#69343=CARTESIAN_POINT('Ctrl Pts',(-26.4658772891907,22.1734517418654,29.8987474197676));
#69344=CARTESIAN_POINT('Ctrl Pts',(-26.4196015840391,22.0829578856508,29.905008776399));
#69345=CARTESIAN_POINT('Ctrl Pts',(-26.3733462169056,21.9925038011844,29.911267381185));
#69346=CARTESIAN_POINT('Ctrl Pts',(-26.3227914617942,21.9042032072897,29.917525985971));
#69347=CARTESIAN_POINT('Ctrl Pts',(-26.2681682537503,21.8184754991925,29.9237845907571));
#69348=CARTESIAN_POINT('Ctrl Pts',(-26.2127361686776,21.7314783091976,29.9301358748606));
#69349=CARTESIAN_POINT('Ctrl Pts',(-26.1531143575681,21.6471312129612,29.9364871589642));
#69350=CARTESIAN_POINT('Ctrl Pts',(-26.0895909161889,21.565843770493,29.9428384430678));
#69351=CARTESIAN_POINT('Ctrl Pts',(-26.0269887177682,21.4857351918013,29.9490976182486));
#69352=CARTESIAN_POINT('Ctrl Pts',(-25.9605976006371,21.4085984170733,29.9553567934293));
#69353=CARTESIAN_POINT('Ctrl Pts',(-25.8907344422317,21.3347927624936,29.9616159686101));
#69354=CARTESIAN_POINT('Ctrl Pts',(-25.8193291428703,21.2593579413358,29.9680133071751));
#69355=CARTESIAN_POINT('Ctrl Pts',(-25.744297009417,21.1874033784249,29.9744106457401));
#69356=CARTESIAN_POINT('Ctrl Pts',(-25.6660158720703,21.1192726778039,29.980807984305));
#69357=CARTESIAN_POINT('Ctrl Pts',(-25.5877347347236,21.0511419771829,29.98720532287));
#69358=CARTESIAN_POINT('Ctrl Pts',(-25.5062049653236,20.9868354125613,29.993602661435));
#69359=CARTESIAN_POINT('Ctrl Pts',(-25.421839063434,20.9266516823442,30.));
#69360=CARTESIAN_POINT('Ctrl Pts',(-22.0750360153459,26.4155367745562,29.4036987823186));
#69361=CARTESIAN_POINT('Ctrl Pts',(-22.163538723818,26.4611031638611,29.4098802346134));
#69362=CARTESIAN_POINT('Ctrl Pts',(-22.2543048787986,26.5026426058483,29.4160616869082));
#69363=CARTESIAN_POINT('Ctrl Pts',(-22.3469329220167,26.5399246674752,29.422243139203));
#69364=CARTESIAN_POINT('Ctrl Pts',(-22.4394383465509,26.5771573760426,29.4284164086461));
#69365=CARTESIAN_POINT('Ctrl Pts',(-22.533800361804,26.6101437469483,29.4345896780891));
#69366=CARTESIAN_POINT('Ctrl Pts',(-22.6295932389525,26.6386993952793,29.4407629475322));
#69367=CARTESIAN_POINT('Ctrl Pts',(-22.7252873456082,26.6672256003411,29.4469298518165));
#69368=CARTESIAN_POINT('Ctrl Pts',(-22.8224089681871,26.6913300432624,29.4530967561009));
#69369=CARTESIAN_POINT('Ctrl Pts',(-22.9205137248114,26.7108769316516,29.4592636603853));
#69370=CARTESIAN_POINT('Ctrl Pts',(-23.0185500479327,26.7304101850031,29.4654262629123));
#69371=CARTESIAN_POINT('Ctrl Pts',(-23.1175677183753,26.7453921203669,29.4715888654392));
#69372=CARTESIAN_POINT('Ctrl Pts',(-23.2171094256828,26.755737398827,29.4777514679662));
#69373=CARTESIAN_POINT('Ctrl Pts',(-23.3166154028359,26.7660789638848,29.4839118584481));
#69374=CARTESIAN_POINT('Ctrl Pts',(-23.416644613055,26.7717871346705,29.49007224893));
#69375=CARTESIAN_POINT('Ctrl Pts',(-23.5167327130705,26.7728282071841,29.4962326394119));
#69376=CARTESIAN_POINT('Ctrl Pts',(-23.6168114130105,26.7738691819223,29.5023924513222));
#69377=CARTESIAN_POINT('Ctrl Pts',(-23.7169485590095,26.7702439254885,29.5085522632325));
#69378=CARTESIAN_POINT('Ctrl Pts',(-23.8166788722726,26.7619708517755,29.5147120751428));
#69379=CARTESIAN_POINT('Ctrl Pts',(-23.9164262500222,26.7536963624874,29.5208729410358));
#69380=CARTESIAN_POINT('Ctrl Pts',(-24.0157662254474,26.7407725118116,29.5270338069288));
#69381=CARTESIAN_POINT('Ctrl Pts',(-24.1142386955665,26.7232695769463,29.5331946728219));
#69382=CARTESIAN_POINT('Ctrl Pts',(-24.2128171516534,26.7057478036637,29.5393621696578));
#69383=CARTESIAN_POINT('Ctrl Pts',(-24.3105258111033,26.6836371806377,29.5455296664938));
#69384=CARTESIAN_POINT('Ctrl Pts',(-24.4069149246519,26.6570591087105,29.5516971633298));
#69385=CARTESIAN_POINT('Ctrl Pts',(-24.5033587057452,26.6304659629034,29.557868158091));
#69386=CARTESIAN_POINT('Ctrl Pts',(-24.5984810390793,26.5994004562953,29.5640391528522));
#69387=CARTESIAN_POINT('Ctrl Pts',(-24.6918494769263,26.5640332100344,29.5702101476134));
#69388=CARTESIAN_POINT('Ctrl Pts',(-24.7853725540406,26.5286073876082,29.5763913629387));
#69389=CARTESIAN_POINT('Ctrl Pts',(-24.8771355361964,26.4888657665696,29.5825725782641));
#69390=CARTESIAN_POINT('Ctrl Pts',(-24.9667278895851,26.4450262919366,29.5887537935894));
#69391=CARTESIAN_POINT('Ctrl Pts',(-25.0318187870004,26.4131759091958,29.593244588143));
#69392=CARTESIAN_POINT('Ctrl Pts',(-25.0957644355923,26.3791635199644,29.5977353826967));
#69393=CARTESIAN_POINT('Ctrl Pts',(-25.1584170365697,26.3430870215554,29.6022261772503));
#69394=CARTESIAN_POINT('Ctrl Pts',(-25.243559258323,26.2940605936067,29.6083289761727));
#69395=CARTESIAN_POINT('Ctrl Pts',(-25.32662678499,26.241039450202,29.6144317750951));
#69396=CARTESIAN_POINT('Ctrl Pts',(-25.4072140012169,26.1842251327681,29.6205345740176));
#69397=CARTESIAN_POINT('Ctrl Pts',(-25.4876901347248,26.127489129106,29.6266289607435));
#69398=CARTESIAN_POINT('Ctrl Pts',(-25.5656923893407,26.0669705912239,29.6327233474695));
#69399=CARTESIAN_POINT('Ctrl Pts',(-25.6408399464524,26.0029167614156,29.6388177341954));
#69400=CARTESIAN_POINT('Ctrl Pts',(-25.7159073224964,25.938931275871,29.6449056183223));
#69401=CARTESIAN_POINT('Ctrl Pts',(-25.788125716647,25.8714182800427,29.6509935024491));
#69402=CARTESIAN_POINT('Ctrl Pts',(-25.8571444259622,25.8006674602486,29.657081386576));
#69403=CARTESIAN_POINT('Ctrl Pts',(-25.9261154992051,25.7299654720134,29.6631650689018));
#69404=CARTESIAN_POINT('Ctrl Pts',(-25.9918909646655,25.6560304161728,29.6692487512276));
#69405=CARTESIAN_POINT('Ctrl Pts',(-26.054155056627,25.5791906056963,29.6753324335534));
#69406=CARTESIAN_POINT('Ctrl Pts',(-26.116397200168,25.5023778816577,29.6814139713491));
#69407=CARTESIAN_POINT('Ctrl Pts',(-26.1751301479751,25.4226627812701,29.6874955091447));
#69408=CARTESIAN_POINT('Ctrl Pts',(-26.2300774405538,25.3404078379053,29.6935770469404));
#69409=CARTESIAN_POINT('Ctrl Pts',(-26.2850208376939,25.2581587259301,29.6996581535911));
#69410=CARTESIAN_POINT('Ctrl Pts',(-26.3361788655351,25.173370498625,29.7057392602417));
#69411=CARTESIAN_POINT('Ctrl Pts',(-26.383318215777,25.0864349401901,29.7118203668923));
#69412=CARTESIAN_POINT('Ctrl Pts',(-26.4304675000564,24.9994810611572,29.7179027550612));
#69413=CARTESIAN_POINT('Ctrl Pts',(-26.4735962130561,24.9103793435768,29.7239851432301));
#69414=CARTESIAN_POINT('Ctrl Pts',(-26.5125173981894,24.8195454148493,29.730067531399));
#69415=CARTESIAN_POINT('Ctrl Pts',(-26.5514865212595,24.7285996089753,29.7361574110443));
#69416=CARTESIAN_POINT('Ctrl Pts',(-26.5862375940756,24.6359177420117,29.7422472906897));
#69417=CARTESIAN_POINT('Ctrl Pts',(-26.6166322300379,24.5419344908351,29.748337170335));
#69418=CARTESIAN_POINT('Ctrl Pts',(-26.6470459155989,24.4478923363959,29.7544308667644));
#69419=CARTESIAN_POINT('Ctrl Pts',(-26.6730976151406,24.3525476038542,29.7605245631938));
#69420=CARTESIAN_POINT('Ctrl Pts',(-26.6946997582596,24.2563468609769,29.7666182596232));
#69421=CARTESIAN_POINT('Ctrl Pts',(-26.7163432303414,24.1599620679845,29.7727236144401));
#69422=CARTESIAN_POINT('Ctrl Pts',(-26.7335200676174,24.0627184319362,29.7788289692569));
#69423=CARTESIAN_POINT('Ctrl Pts',(-26.7461943958854,23.9650695554648,29.7849343240737));
#69424=CARTESIAN_POINT('Ctrl Pts',(-26.7573897579376,23.8788153175311,29.7903272455908));
#69425=CARTESIAN_POINT('Ctrl Pts',(-26.7650728676828,23.7922451571525,29.7957201671079));
#69426=CARTESIAN_POINT('Ctrl Pts',(-26.76925281896,23.705670397728,29.801113088625));
#69427=CARTESIAN_POINT('Ctrl Pts',(-26.7717486731212,23.6539765000638,29.8043332088409));
#69428=CARTESIAN_POINT('Ctrl Pts',(-26.7729988436791,23.6022338915603,29.8075533290569));
#69429=CARTESIAN_POINT('Ctrl Pts',(-26.7730025235471,23.5504816870455,29.8107734492728));
#69430=CARTESIAN_POINT('Ctrl Pts',(-24.9806647809486,26.4319136911417,-75.413296538515));
#69431=CARTESIAN_POINT('Ctrl Pts',(-25.9409444120173,25.9552456614925,-75.3470009013901));
#69432=CARTESIAN_POINT('Ctrl Pts',(-27.3306922290377,23.9746675204515,-75.2144096271402));
#69433=CARTESIAN_POINT('Ctrl Pts',(-25.9479925434464,20.5921055094508,-75.0155227157653));
#69434=CARTESIAN_POINT('Ctrl Pts',(-22.358936684886,19.9375333945402,-74.8166358043905));
#69435=CARTESIAN_POINT('Ctrl Pts',(-19.8661618148865,22.5978429125412,-74.6177488930155));
#69436=CARTESIAN_POINT('Ctrl Pts',(-20.7579317754914,26.1359023573449,-74.4188619816407));
#69437=CARTESIAN_POINT('Ctrl Pts',(-24.2160425247577,27.2966133380363,-74.2199750702657));
#69438=CARTESIAN_POINT('Ctrl Pts',(-27.0621185490293,25.0154538166582,-74.0210881588908));
#69439=CARTESIAN_POINT('Ctrl Pts',(-26.6812093500516,21.3875186376235,-73.822201247516));
#69440=CARTESIAN_POINT('Ctrl Pts',(-23.4231517443953,19.7471537304636,-73.623314336141));
#69441=CARTESIAN_POINT('Ctrl Pts',(-20.2819231727274,21.6014076203184,-73.4244274247662));
#69442=CARTESIAN_POINT('Ctrl Pts',(-20.1439940678548,25.2465411790391,-73.2255405133912));
#69443=CARTESIAN_POINT('Ctrl Pts',(-23.1361372768816,27.3328994068108,-73.0266536020164));
#69444=CARTESIAN_POINT('Ctrl Pts',(-26.5088122156722,25.9433416994471,-72.8277666906415));
#69445=CARTESIAN_POINT('Ctrl Pts',(-27.1628243388303,22.3547295650974,-72.6288797792667));
#69446=CARTESIAN_POINT('Ctrl Pts',(-24.4971878424663,19.8647061127295,-72.4299928678917));
#69447=CARTESIAN_POINT('Ctrl Pts',(-20.9613988367147,20.7613849855078,-72.2311059565169));
#69448=CARTESIAN_POINT('Ctrl Pts',(-19.8045464785528,24.2207979213969,-72.0322190451419));
#69449=CARTESIAN_POINT('Ctrl Pts',(-22.0896806113034,27.0640358375917,-71.833332133767));
#69450=CARTESIAN_POINT('Ctrl Pts',(-25.7169563907639,26.678405164599,-71.6344452223922));
#69451=CARTESIAN_POINT('Ctrl Pts',(-27.3532150892751,23.4182672606151,-71.4355583110172));
#69452=CARTESIAN_POINT('Ctrl Pts',(-25.4948736039934,20.2794127282015,-71.2366713996424));
#69453=CARTESIAN_POINT('Ctrl Pts',(-21.8495902465907,20.1461826018379,-71.0377844882675));
#69454=CARTESIAN_POINT('Ctrl Pts',(-19.7670713279998,23.1410041509518,-70.8388975768926));
#69455=CARTESIAN_POINT('Ctrl Pts',(-21.1609751794025,26.5118902488768,-70.6400106655177));
#69456=CARTESIAN_POINT('Ctrl Pts',(-24.7504223377759,27.1612823978862,-70.4411237541428));
#69457=CARTESIAN_POINT('Ctrl Pts',(-27.2370152032886,24.4924442606275,-70.2422368427679));
#69458=CARTESIAN_POINT('Ctrl Pts',(-26.3357857588391,20.9578118113256,-70.0433499313931));
#69459=CARTESIAN_POINT('Ctrl Pts',(-22.8748874532814,19.8054125801717,-69.8444630200181));
#69460=CARTESIAN_POINT('Ctrl Pts',(-20.0345923930747,22.0942037550054,-69.6455761086433));
#69461=CARTESIAN_POINT('Ctrl Pts',(-20.4248909215382,25.7209803027169,-69.4466891972683));
#69462=CARTESIAN_POINT('Ctrl Pts',(-23.6871317827143,27.3530420763928,-69.2478022858935));
#69463=CARTESIAN_POINT('Ctrl Pts',(-26.8235922176786,25.4906626817836,-69.0489153745184));
#69464=CARTESIAN_POINT('Ctrl Pts',(-26.9521310146457,21.8452108789403,-68.8500284631438));
#69465=CARTESIAN_POINT('Ctrl Pts',(-23.9546319175192,19.7665477912599,-68.6511415517687));
#69466=CARTESIAN_POINT('Ctrl Pts',(-20.5855424505331,21.1647885547934,-68.452254640394));
#69467=CARTESIAN_POINT('Ctrl Pts',(-19.9407701821737,24.7550684590997,-68.2533677290189));
#69468=CARTESIAN_POINT('Ctrl Pts',(-22.6128061593865,27.2382246776691,-68.0544808176442));
#69469=CARTESIAN_POINT('Ctrl Pts',(-26.1462758704056,26.3324471825587,-67.8555939062692));
#69470=CARTESIAN_POINT('Ctrl Pts',(-27.2942202396304,22.8700686945109,-67.6567069948944));
#69471=CARTESIAN_POINT('Ctrl Pts',(-25.0017757213758,20.0327214827548,-67.4578200835195));
#69472=CARTESIAN_POINT('Ctrl Pts',(-21.3755044606752,20.4276870675231,-67.2589331721445));
#69473=CARTESIAN_POINT('Ctrl Pts',(-19.7476422890117,23.6920255639724,-67.0600462607698));
#69474=CARTESIAN_POINT('Ctrl Pts',(-21.6140565221925,26.826086664129,-66.8611593493947));
#69475=CARTESIAN_POINT('Ctrl Pts',(-25.2596707257554,26.94993394151,-66.6622724380199));
#69476=CARTESIAN_POINT('Ctrl Pts',(-27.334474543738,23.9497622487199,-66.4633855266449));
#69477=CARTESIAN_POINT('Ctrl Pts',(-25.9318991817683,20.5824749988213,-66.2644986152701));
#69478=CARTESIAN_POINT('Ctrl Pts',(-22.3407924787165,19.9423236755932,-66.0656117038951));
#69479=CARTESIAN_POINT('Ctrl Pts',(-19.8610770190493,22.6175530692006,-65.8667247925203));
#69480=CARTESIAN_POINT('Ctrl Pts',(-20.7714010650008,26.149854188966,-65.6678378811455));
#69481=CARTESIAN_POINT('Ctrl Pts',(-24.2352540010928,27.2933417955719,-65.4689509697706));
#69482=CARTESIAN_POINT('Ctrl Pts',(-27.0696486653545,24.9972477303081,-65.2700640583956));
#69483=CARTESIAN_POINT('Ctrl Pts',(-26.6700166783666,21.3714877624793,-65.0711771470207));
#69484=CARTESIAN_POINT('Ctrl Pts',(-23.4035859529662,19.7478278887697,-64.8722902356459));
#69485=CARTESIAN_POINT('Ctrl Pts',(-20.2719293781416,21.6182738694631,-64.6734033242709));
#69486=CARTESIAN_POINT('Ctrl Pts',(-20.1527738254655,25.264044435969,-64.4745164128962));
#69487=CARTESIAN_POINT('Ctrl Pts',(-23.1556131451224,27.3349855480378,-64.2756295015211));
#69488=CARTESIAN_POINT('Ctrl Pts',(-26.5210926011366,25.9280779105288,-64.0767425901465));
#69489=CARTESIAN_POINT('Ctrl Pts',(-27.1566219190331,22.3361503562165,-63.8778556787712));
#69490=CARTESIAN_POINT('Ctrl Pts',(-24.4782035396653,19.8598797622791,-63.6789687673967));
#69491=CARTESIAN_POINT('Ctrl Pts',(-20.947076861243,20.7747488514217,-63.4800818560215));
#69492=CARTESIAN_POINT('Ctrl Pts',(-19.8080479110658,24.2400704988293,-63.2811949446469));
#69493=CARTESIAN_POINT('Ctrl Pts',(-22.1077877206174,27.0715079213585,-63.0823080332718));
#69494=CARTESIAN_POINT('Ctrl Pts',(-25.7330303907009,26.6672101940093,-62.883421121897));
#69495=CARTESIAN_POINT('Ctrl Pts',(-27.3524852774003,23.3986926494214,-62.6845342105221));
#69496=CARTESIAN_POINT('Ctrl Pts',(-25.4780106469702,20.2694457864832,-62.4856472991471));
#69497=CARTESIAN_POINT('Ctrl Pts',(-21.8320897555359,20.1549821558538,-62.2867603877724));
#69498=CARTESIAN_POINT('Ctrl Pts',(-19.7650147792107,23.1604841291662,-62.0878734763974));
#69499=CARTESIAN_POINT('Ctrl Pts',(-21.1762523621812,26.5241502174909,-61.8889865650226));
#69500=CARTESIAN_POINT('Ctrl Pts',(-24.7689948189127,27.1550564775115,-61.6900996536476));
#69501=CARTESIAN_POINT('Ctrl Pts',(-27.2418164459961,24.4734535482986,-61.4912127422729));
#69502=CARTESIAN_POINT('Ctrl Pts',(-26.3224038288408,20.9435071593643,-61.2923258308977));
#69503=CARTESIAN_POINT('Ctrl Pts',(-22.8556192092779,19.8089387520409,-61.0934389195231));
#69504=CARTESIAN_POINT('Ctrl Pts',(-20.0271437178222,22.1123204971208,-60.8945520081478));
#69505=CARTESIAN_POINT('Ctrl Pts',(-20.436106515947,25.7370398654423,-60.6956650967734));
#69506=CARTESIAN_POINT('Ctrl Pts',(-23.7067054665031,27.3522870830397,-60.4967781853982));
#69507=CARTESIAN_POINT('Ctrl Pts',(-26.8335374349911,25.4737869073209,-60.2978912740235));
#69508=CARTESIAN_POINT('Ctrl Pts',(-26.9433089540025,21.8277217292215,-60.0990043626484));
#69509=CARTESIAN_POINT('Ctrl Pts',(-23.9351493046558,19.7645163120668,-59.9001174512737));
#69510=CARTESIAN_POINT('Ctrl Pts',(-20.5733021548222,21.1800815032499,-59.7012305398987));
#69511=CARTESIAN_POINT('Ctrl Pts',(-19.9470199975653,24.7736329122096,-59.5023436285239));
#69512=CARTESIAN_POINT('Ctrl Pts',(-22.6318030354339,27.2430014770267,-59.3034567171489));
#69513=CARTESIAN_POINT('Ctrl Pts',(-26.1605632886902,26.3190468545622,-59.1045698057741));
#69514=CARTESIAN_POINT('Ctrl Pts',(-27.2906692741222,22.8508050044276,-58.9056828943991));
#69515=CARTESIAN_POINT('Ctrl Pts',(-24.9836494083045,20.0252961284803,-58.7067959830244));
#69516=CARTESIAN_POINT('Ctrl Pts',(-21.3594593448955,20.4389233200691,-58.5079090716493));
#69517=CARTESIAN_POINT('Ctrl Pts',(-19.7484224715237,23.7115982599265,-58.3090221602746));
#69518=CARTESIAN_POINT('Ctrl Pts',(-21.6309450814161,26.8360101554002,-58.1101352488995));
#69519=CARTESIAN_POINT('Ctrl Pts',(-25.277148507678,26.9410893809935,-57.9112483375248));
#69520=CARTESIAN_POINT('Ctrl Pts',(-27.3364809486441,23.9302770376352,-57.7123614261497));
#69521=CARTESIAN_POINT('Ctrl Pts',(-25.9165904936644,20.5702543940817,-57.513474514775));
#69522=CARTESIAN_POINT('Ctrl Pts',(-22.3222360840073,19.9485973768181,-57.3145876034));
#69523=CARTESIAN_POINT('Ctrl Pts',(-19.8563246711497,22.6365560768863,-57.1157006920252));
#69524=CARTESIAN_POINT('Ctrl Pts',(-20.7848197686979,26.1641243502388,-56.9168137806502));
#69525=CARTESIAN_POINT('Ctrl Pts',(-24.2545131054074,27.2897660421322,-56.7179268692754));
#69526=CARTESIAN_POINT('Ctrl Pts',(-27.0770506863242,24.9791118763931,-56.5190399579004));
#69527=CARTESIAN_POINT('Ctrl Pts',(-26.6587597863081,21.3554571201701,-56.3201530465256));
#69528=CARTESIAN_POINT('Ctrl Pts',(-23.3840142772543,19.7486332591741,-56.1212661351506));
#69529=CARTESIAN_POINT('Ctrl Pts',(-20.2620276293511,21.6351751854637,-55.9223792237759));
#69530=CARTESIAN_POINT('Ctrl Pts',(-20.161640871205,25.2815108211564,-55.7234923124009));
#69531=CARTESIAN_POINT('Ctrl Pts',(-23.1751009221589,27.3369668753301,-55.5246054010261));
#69532=CARTESIAN_POINT('Ctrl Pts',(-26.5332934946646,25.9127535081333,-55.3257184896511));
#69533=CARTESIAN_POINT('Ctrl Pts',(-27.1503243423656,22.3176020506395,-55.1268315782763));
#69534=CARTESIAN_POINT('Ctrl Pts',(-24.4591944318132,19.8551518737089,-54.9279446669013));
#69535=CARTESIAN_POINT('Ctrl Pts',(-20.932823980616,20.7881859085956,-54.7290577555265));
#69536=CARTESIAN_POINT('Ctrl Pts',(-19.8116484465149,24.259324985479,-54.5301708441516));
#69537=CARTESIAN_POINT('Ctrl Pts',(-22.1259330853401,27.0788865967642,-54.3312839327767));
#69538=CARTESIAN_POINT('Ctrl Pts',(-25.7490465329901,26.6559326810817,-54.1323970214018));
#69539=CARTESIAN_POINT('Ctrl Pts',(-27.3516547204373,23.3791220263656,-53.9335101100269));
#69540=CARTESIAN_POINT('Ctrl Pts',(-25.4610966021844,20.2595657965723,-53.7346231986521));
#69541=CARTESIAN_POINT('Ctrl Pts',(-21.8146347960108,20.1638716721309,-53.5357362872771));
#69542=CARTESIAN_POINT('Ctrl Pts',(-19.7630585328137,23.1799744398794,-53.3368493759022));
#69543=CARTESIAN_POINT('Ctrl Pts',(-21.1915924534886,26.5363313796006,-53.1379624645274));
#69544=CARTESIAN_POINT('Ctrl Pts',(-24.7875350046384,27.1487350358311,-52.9390755531523));
#69545=CARTESIAN_POINT('Ctrl Pts',(-27.2465198674066,24.4544383717626,-52.7401886417776));
#69546=CARTESIAN_POINT('Ctrl Pts',(-26.3089484404444,20.9292715829881,-52.5413017304026));
#69547=CARTESIAN_POINT('Ctrl Pts',(-22.836369372182,19.8125640635364,-52.3424148190278));
#69548=CARTESIAN_POINT('Ctrl Pts',(-20.0197884002008,22.1304753425994,-52.1435279076528));
#69549=CARTESIAN_POINT('Ctrl Pts',(-20.4474046310663,25.7530414811861,-51.944640996278));
#69550=CARTESIAN_POINT('Ctrl Pts',(-23.7262750044905,27.3514313408934,-51.7457540849031));
#69551=CARTESIAN_POINT('Ctrl Pts',(-26.8433956496595,25.456860161762,-51.5468671735283));
#69552=CARTESIAN_POINT('Ctrl Pts',(-26.9343969819104,21.8102782242672,-51.3479802621533));
#69553=CARTESIAN_POINT('Ctrl Pts',(-23.9156564925452,19.7625851498047,-51.1490933507783));
#69554=CARTESIAN_POINT('Ctrl Pts',(-20.5611407443049,21.1954372580634,-50.9502064394036));
#69555=CARTESIAN_POINT('Ctrl Pts',(-19.953365293789,24.7921649473783,-50.7513195280286));
#69556=CARTESIAN_POINT('Ctrl Pts',(-22.6508242491617,27.2476804234881,-50.5524326166538));
#69557=CARTESIAN_POINT('Ctrl Pts',(-26.1747815372389,26.3055731572274,-50.3535457052789));
#69558=CARTESIAN_POINT('Ctrl Pts',(-27.2870191925844,22.8315598487661,-50.154658793904));
#69559=CARTESIAN_POINT('Ctrl Pts',(-24.9654851121375,20.017964180825,-49.955771882529));
#69560=CARTESIAN_POINT('Ctrl Pts',(-21.3434722821983,20.4502420186684,-49.7568849711542));
#69561=CARTESIAN_POINT('Ctrl Pts',(-19.7493033974357,23.7311666804351,-49.5579980597793));
#69562=CARTESIAN_POINT('Ctrl Pts',(-21.6478844997144,26.8458465784991,-49.3591111484045));
#69563=CARTESIAN_POINT('Ctrl Pts',(-25.2945805291721,26.932154967846,-49.1602242370294));
#69564=CARTESIAN_POINT('Ctrl Pts',(-27.3383870235728,23.9107817564105,-48.9613373256547));
#69565=CARTESIAN_POINT('Ctrl Pts',(-25.9012191007766,20.5581127552981,-48.7624504142797));
#69566=CARTESIAN_POINT('Ctrl Pts',(-22.3037122300878,19.9549665170764,-48.5635635029049));
#69567=CARTESIAN_POINT('Ctrl Pts',(-19.8516702073867,22.6555832963033,-48.36467659153));
#69568=CARTESIAN_POINT('Ctrl Pts',(-20.7983117526562,26.1783252474125,-48.1657896801551));
#69569=CARTESIAN_POINT('Ctrl Pts',(-24.2737535477609,27.2860911965973,-47.9669027687802));
#69570=CARTESIAN_POINT('Ctrl Pts',(-27.0843592518706,24.9609381596209,-47.7680158574053));
#69571=CARTESIAN_POINT('Ctrl Pts',(-26.6474205229744,21.339484636997,-47.5691289460303));
#69572=CARTESIAN_POINT('Ctrl Pts',(-23.3644470066332,19.7495393673931,-47.3702420346555));
#69573=CARTESIAN_POINT('Ctrl Pts',(-20.2522130141123,21.6521272484466,-47.1713551232806));
#69574=CARTESIAN_POINT('Ctrl Pts',(-20.1705977106109,25.29893133032,-46.9724682119057));
#69575=CARTESIAN_POINT('Ctrl Pts',(-23.1945986402101,27.3388478597686,-46.7735813005308));
#69576=CARTESIAN_POINT('Ctrl Pts',(-26.545415341606,25.8973665026288,-46.5746943891558));
#69577=CARTESIAN_POINT('Ctrl Pts',(-27.143931368621,22.2990864086478,-46.3758074777811));
#69578=CARTESIAN_POINT('Ctrl Pts',(-24.4401612382193,19.8505219003528,-46.1769205664061));
#69579=CARTESIAN_POINT('Ctrl Pts',(-20.9186404583367,20.8016961568323,-45.9780336550313));
#69580=CARTESIAN_POINT('Ctrl Pts',(-19.8153480499607,24.2785606826592,-45.7791467436562));
#69581=CARTESIAN_POINT('Ctrl Pts',(-22.1441161926188,27.0861717680974,-45.5802598322816));
#69582=CARTESIAN_POINT('Ctrl Pts',(-25.765004410186,26.6445728717935,-45.3813729209065));
#69583=CARTESIAN_POINT('Ctrl Pts',(-27.3507234314122,23.3595559380386,-45.1824860095318));
#69584=CARTESIAN_POINT('Ctrl Pts',(-25.444131922592,20.2497730054484,-44.9835990981568));
#69585=CARTESIAN_POINT('Ctrl Pts',(-21.7972258280291,20.1728509229612,-44.7847121867819));
#69586=CARTESIAN_POINT('Ctrl Pts',(-19.7612026419805,23.1994745624656,-44.585825275407));
#69587=CARTESIAN_POINT('Ctrl Pts',(-21.2069950461263,26.5484334146239,-44.3869383640322));
#69588=CARTESIAN_POINT('Ctrl Pts',(-24.8060424040373,27.1423182391883,-44.1880514526573));
#69589=CARTESIAN_POINT('Ctrl Pts',(-27.2511253426879,24.4353992355138,-43.9891645412823));
#69590=CARTESIAN_POINT('Ctrl Pts',(-26.2954199503044,20.9151054590935,-43.7902776299075));
#69591=CARTESIAN_POINT('Ctrl Pts',(-22.8171384520326,19.8162884187658,-43.5913907185326));
#69592=CARTESIAN_POINT('Ctrl Pts',(-20.0125266351462,22.1486678102704,-43.3925038071577));
#69593=CARTESIAN_POINT('Ctrl Pts',(-20.4587849674954,25.7689847259758,-43.1936168957828));
#69594=CARTESIAN_POINT('Ctrl Pts',(-23.7458398781184,27.3504748726044,-42.9947299844079));
#69595=CARTESIAN_POINT('Ctrl Pts',(-26.8531666004498,25.4398828936568,-42.795843073033));
#69596=CARTESIAN_POINT('Ctrl Pts',(-26.9253953345269,21.7928808262996,-42.5969561616581));
#69597=CARTESIAN_POINT('Ctrl Pts',(-23.8961539977194,19.7607543556508,-42.3980692502833));
#69598=CARTESIAN_POINT('Ctrl Pts',(-20.5490585412428,21.2108554123249,-42.1991823389084));
#69599=CARTESIAN_POINT('Ctrl Pts',(-19.9598059027029,24.8106640735329,-42.0002954275335));
#69600=CARTESIAN_POINT('Ctrl Pts',(-22.6698692965332,27.2522613930669,-41.8014085161585));
#69601=CARTESIAN_POINT('Ctrl Pts',(-26.1889302392874,26.2920264475898,-41.6025216047838));
#69602=CARTESIAN_POINT('Ctrl Pts',(-27.2832700917394,22.8123337374975,-41.4036346934087));
#69603=CARTESIAN_POINT('Ctrl Pts',(-24.9472833142043,20.0107258340757,-41.204747782034));
#69604=CARTESIAN_POINT('Ctrl Pts',(-21.3275436962196,20.4616428633906,-41.0058608706589));
#69605=CARTESIAN_POINT('Ctrl Pts',(-19.7502850434045,23.7507303069612,-40.8069739592842));
#69606=CARTESIAN_POINT('Ctrl Pts',(-21.6648743282153,26.8555956727737,-40.6080870479092));
#69607=CARTESIAN_POINT('Ctrl Pts',(-25.3119663283127,26.9231309388175,-40.4092001365344));
#69608=CARTESIAN_POINT('Ctrl Pts',(-27.3401927180156,23.8912769216447,-40.2103132251595));
#69609=CARTESIAN_POINT('Ctrl Pts',(-25.8857854104263,20.5460504042074,-40.0114263137845));
#69610=CARTESIAN_POINT('Ctrl Pts',(-22.2852214078152,19.9614309275945,-39.8125394024097));
#69611=CARTESIAN_POINT('Ctrl Pts',(-19.8471137510971,22.6746342232557,-39.6136524910347));
#69612=CARTESIAN_POINT('Ctrl Pts',(-20.8118766593559,26.1924565041821,-39.4147655796599));
#69613=CARTESIAN_POINT('Ctrl Pts',(-24.2929748183074,27.2823173563459,-39.215878668285));
#69614=CARTESIAN_POINT('Ctrl Pts',(-27.0915741683264,24.9427270615707,-39.01699175691));
#69615=CARTESIAN_POINT('Ctrl Pts',(-26.635999188841,21.3235707362095,-38.8181048455351));
#69616=CARTESIAN_POINT('Ctrl Pts',(-23.3448846596095,19.7505461894159,-38.6192179341603));
#69617=CARTESIAN_POINT('Ctrl Pts',(-20.2424857924997,21.6691296092051,-38.4203310227854));
#69618=CARTESIAN_POINT('Ctrl Pts',(-20.179644106339,25.3163055018397,-38.2214441114106));
#69619=CARTESIAN_POINT('Ctrl Pts',(-23.2141057826128,27.3406284515096,-38.0225572000355));
#69620=CARTESIAN_POINT('Ctrl Pts',(-26.5574578207479,25.8819173017506,-37.8236702886608));
#69621=CARTESIAN_POINT('Ctrl Pts',(-27.1374431672049,22.2806039208811,-37.6247833772859));
#69622=CARTESIAN_POINT('Ctrl Pts',(-24.4211044632376,19.8459899648987,-37.425896465911));
#69623=CARTESIAN_POINT('Ctrl Pts',(-20.9045266702496,20.8152792381283,-37.227009554536));
#69624=CARTESIAN_POINT('Ctrl Pts',(-19.8191466233683,24.2977770806498,-37.0281226431611));
#69625=CARTESIAN_POINT('Ctrl Pts',(-22.1623365606255,27.0933632423109,-36.8292357317863));
#69626=CARTESIAN_POINT('Ctrl Pts',(-25.7809035994259,26.6331310671643,-36.6303488204115));
#69627=CARTESIAN_POINT('Ctrl Pts',(-27.349691435003,23.3399949029159,-36.4314619090365));
#69628=CARTESIAN_POINT('Ctrl Pts',(-25.4271170577346,20.2400676726077,-36.2325749976617));
#69629=CARTESIAN_POINT('Ctrl Pts',(-21.7798633129051,20.1819196704065,-36.0336880862867));
#69630=CARTESIAN_POINT('Ctrl Pts',(-19.7594471558902,23.2189839801978,-35.8348011749118));
#69631=CARTESIAN_POINT('Ctrl Pts',(-21.222459731946,26.5604560018729,-35.635914263537));
#69632=CARTESIAN_POINT('Ctrl Pts',(-24.8245165266878,27.1358062576196,-35.4370273521619));
#69633=CARTESIAN_POINT('Ctrl Pts',(-27.2556327498007,24.416336644064,-35.2381404407871));
#69634=CARTESIAN_POINT('Ctrl Pts',(-26.2818187169079,20.9010091630639,-35.0392535294122));
#69635=CARTESIAN_POINT('Ctrl Pts',(-22.7979269584237,19.8201117190387,-34.8403666180374));
#69636=CARTESIAN_POINT('Ctrl Pts',(-20.0053586150854,22.1668974180574,-34.6414797066625));
#69637=CARTESIAN_POINT('Ctrl Pts',(-20.4702472236707,25.7848691773366,-34.4425927952876));
#69638=CARTESIAN_POINT('Ctrl Pts',(-23.7653995689437,27.3494177035177,-34.2437058839126));
#69639=CARTESIAN_POINT('Ctrl Pts',(-26.8628500284451,25.4228555528801,-34.0448189725379));
#69640=CARTESIAN_POINT('Ctrl Pts',(-26.9163042503836,21.7755299963262,-33.8459320611629));
#69641=CARTESIAN_POINT('Ctrl Pts',(-23.8766423369686,19.7590239781184,-33.647045149788));
#69642=CARTESIAN_POINT('Ctrl Pts',(-20.5370558657983,21.226335557474,-33.4481582384131));
#69643=CARTESIAN_POINT('Ctrl Pts',(-19.9663416536393,24.8291298004711,-33.2492713270383));
#69644=CARTESIAN_POINT('Ctrl Pts',(-22.6889376728801,27.2567442643736,-33.0503844156634));
#69645=CARTESIAN_POINT('Ctrl Pts',(-26.2030090199139,26.2784070846188,-32.8514975042885));
#69646=CARTESIAN_POINT('Ctrl Pts',(-27.2794220709334,22.7931271800876,-32.6526105929135));
#69647=CARTESIAN_POINT('Ctrl Pts',(-24.9290444968282,20.003581280039,-32.4537236815387));
#69648=CARTESIAN_POINT('Ctrl Pts',(-21.3116740090453,20.4731255521286,-32.2548367701638));
#69649=CARTESIAN_POINT('Ctrl Pts',(-19.7513673834177,23.770288621095,-32.055949858789));
#69650=CARTESIAN_POINT('Ctrl Pts',(-21.6819141167111,26.8652571798861,-31.857062947414));
#69651=CARTESIAN_POINT('Ctrl Pts',(-25.3293054443993,26.9140175330327,-31.6581760360392));
#69652=CARTESIAN_POINT('Ctrl Pts',(-27.341897984124,23.8717630501896,-31.4592891246643));
#69653=CARTESIAN_POINT('Ctrl Pts',(-25.8702898315857,20.5340676604459,-31.2604022132894));
#69654=CARTESIAN_POINT('Ctrl Pts',(-22.2667641071716,19.9679904370741,-31.0615153019145));
#69655=CARTESIAN_POINT('Ctrl Pts',(-19.842655423021,22.6937083529194,-30.8626283905396));
#69656=CARTESIAN_POINT('Ctrl Pts',(-20.8255141293454,26.2065177460884,-30.6637414791646));
#69657=CARTESIAN_POINT('Ctrl Pts',(-24.3121764077089,27.2784446213798,-30.4648545677898));
#69658=CARTESIAN_POINT('Ctrl Pts',(-27.0986952445063,24.924479064812,-30.2659676564149));
#69659=CARTESIAN_POINT('Ctrl Pts',(-26.6244960865576,21.3077158395049,-30.06708074504));
#69660=CARTESIAN_POINT('Ctrl Pts',(-23.325327754559,19.751653698563,-29.8681938336652));
#69661=CARTESIAN_POINT('Ctrl Pts',(-20.2328462222715,21.6861818171993,-29.6693069222903));
#69662=CARTESIAN_POINT('Ctrl Pts',(-20.188779818672,25.3336328753231,-29.4704200109154));
#69663=CARTESIAN_POINT('Ctrl Pts',(-23.2336218324535,27.34230860337,-29.2715330995405));
#69664=CARTESIAN_POINT('Ctrl Pts',(-26.5694206129811,25.8664063148816,-29.0726461881655));
#69665=CARTESIAN_POINT('Ctrl Pts',(-27.1308599100455,22.2621550771006,-28.8737592767907));
#69666=CARTESIAN_POINT('Ctrl Pts',(-24.4020246118471,19.841556187437,-28.6748723654158));
#69667=CARTESIAN_POINT('Ctrl Pts',(-20.8904829903512,20.8289347925503,-28.4759854540409));
#69668=CARTESIAN_POINT('Ctrl Pts',(-19.8230440660809,24.3169736702418,-28.2770985426659));
#69669=CARTESIAN_POINT('Ctrl Pts',(-22.1805937065447,27.1004608288402,-28.0782116312911));
#69670=CARTESIAN_POINT('Ctrl Pts',(-25.796743679403,26.6216075703866,-27.8793247199162));
#69671=CARTESIAN_POINT('Ctrl Pts',(-27.348558758556,23.3204394393384,-27.6804378085414));
#69672=CARTESIAN_POINT('Ctrl Pts',(-25.4100524584835,20.2304500552283,-27.4815508971664));
#69673=CARTESIAN_POINT('Ctrl Pts',(-21.7625477107219,20.1910776741573,-27.2826639857916));
#69674=CARTESIAN_POINT('Ctrl Pts',(-19.7577921210606,23.2385021761025,-27.0837770744166));
#69675=CARTESIAN_POINT('Ctrl Pts',(-21.2379861011544,26.5723988227651,-26.8848901630418));
#69676=CARTESIAN_POINT('Ctrl Pts',(-24.8429568830509,27.1291992636838,-26.6860032516668));
#69677=CARTESIAN_POINT('Ctrl Pts',(-27.2600419693051,24.3972511025463,-26.4871163402919));
#69678=CARTESIAN_POINT('Ctrl Pts',(-26.2681451006692,20.8869830684321,-26.288229428917));
#69679=CARTESIAN_POINT('Ctrl Pts',(-22.7787354004341,19.8240338630426,-26.0893425175421));
#69680=CARTESIAN_POINT('Ctrl Pts',(-19.9982845299614,22.1851636829005,-25.8904556061674));
#69681=CARTESIAN_POINT('Ctrl Pts',(-20.4817910958577,25.8006944143518,-25.6915686947925));
#69682=CARTESIAN_POINT('Ctrl Pts',(-23.784953558661,27.348259861647,-25.4926817834176));
#69683=CARTESIAN_POINT('Ctrl Pts',(-26.8724456770472,25.4057785906337,-25.2937948720426));
#69684=CARTESIAN_POINT('Ctrl Pts',(-26.9071239703822,21.7582261941211,-25.0949079606678));
#69685=CARTESIAN_POINT('Ctrl Pts',(-23.8571220273254,19.7573940630605,-24.8960210492929));
#69686=CARTESIAN_POINT('Ctrl Pts',(-20.5251330360261,21.2418772833075,-24.6971341379179));
#69687=CARTESIAN_POINT('Ctrl Pts',(-19.9729723734095,24.8475616388761,-24.498247226543));
#69688=CARTESIAN_POINT('Ctrl Pts',(-22.708028872916,27.2611289186181,-24.2993603151682));
#69689=CARTESIAN_POINT('Ctrl Pts',(-26.2170175060494,26.2647154292095,-24.1004734037934));
#69690=CARTESIAN_POINT('Ctrl Pts',(-27.2754752321336,22.7739406854847,-23.9015864924183));
#69691=CARTESIAN_POINT('Ctrl Pts',(-24.9107691433134,19.9965307080362,-23.7026995810436));
#69692=CARTESIAN_POINT('Ctrl Pts',(-21.2958636412011,20.4846897806064,-23.5038126696685));
#69693=CARTESIAN_POINT('Ctrl Pts',(-19.7525503887947,23.7898411045674,-23.3049257582937));
#69694=CARTESIAN_POINT('Ctrl Pts',(-21.6990034136701,26.8748308438189,-23.1060388469188));
#69695=CARTESIAN_POINT('Ctrl Pts',(-25.3465974179686,26.9048149919848,-22.9071519355439));
#69696=CARTESIAN_POINT('Ctrl Pts',(-27.3435027767108,23.8522406591371,-22.7082650241691));
#69697=CARTESIAN_POINT('Ctrl Pts',(-25.8547327748668,20.5221648415401,-22.5093781127942));
#69698=CARTESIAN_POINT('Ctrl Pts',(-22.2483408172507,19.9746448716971,-22.3104912014193));
#69699=CARTESIAN_POINT('Ctrl Pts',(-19.838295341298,22.7128051798555,-22.1116042900445));
#69700=CARTESIAN_POINT('Ctrl Pts',(-20.8392238012498,26.2205086005273,-21.9127173786694));
#69701=CARTESIAN_POINT('Ctrl Pts',(-24.3313578071489,27.274473094321,-21.7138304672947));
#69702=CARTESIAN_POINT('Ctrl Pts',(-27.1057222917111,24.9061946528926,-21.5149435559197));
#69703=CARTESIAN_POINT('Ctrl Pts',(-26.6129115209411,21.2919203670162,-21.3160566445449));
#69704=CARTESIAN_POINT('Ctrl Pts',(-23.3057768097138,19.752861865487,-21.1171697331699));
#69705=CARTESIAN_POINT('Ctrl Pts',(-20.2232945588633,21.7032834205684,-20.918282821795));
#69706=CARTESIAN_POINT('Ctrl Pts',(-20.1980046055256,25.350912991618,-20.7193959104201));
#69707=CARTESIAN_POINT('Ctrl Pts',(-23.2531462725832,27.3438882708278,-20.5205089990453));
#69708=CARTESIAN_POINT('Ctrl Pts',(-26.5813034013074,25.8508339530424,-20.3216220876704));
#69709=CARTESIAN_POINT('Ctrl Pts',(-27.1241817715908,22.243740366176,-20.1227351762954));
#69710=CARTESIAN_POINT('Ctrl Pts',(-24.3829221896386,19.8372206854567,-19.9238482649207));
#69711=CARTESIAN_POINT('Ctrl Pts',(-20.8765097907801,20.8426624582443,-19.7249613535456));
#69712=CARTESIAN_POINT('Ctrl Pts',(-19.8270402748213,24.3361499427514,-19.5260744421708));
#69713=CARTESIAN_POINT('Ctrl Pts',(-22.1988871465868,27.107464339609,-19.3271875307959));
#69714=CARTESIAN_POINT('Ctrl Pts',(-25.8125242303759,26.6100026868178,-19.128300619421));
#69715=CARTESIAN_POINT('Ctrl Pts',(-27.3473254320858,23.3008900655,-18.9294137080461));
#69716=CARTESIAN_POINT('Ctrl Pts',(-25.3929385770275,20.2209204081642,-18.7305267966713));
#69717=CARTESIAN_POINT('Ctrl Pts',(-21.7452794803202,20.2003246915387,-18.5316398852963));
#69718=CARTESIAN_POINT('Ctrl Pts',(-19.7562375813478,23.2580286329736,-18.3327529739214));
#69719=CARTESIAN_POINT('Ctrl Pts',(-21.2535737423235,26.5842615608319,-18.1338660625466));
#69720=CARTESIAN_POINT('Ctrl Pts',(-24.8613629844814,27.1224974324572,-17.9349791511717));
#69721=CARTESIAN_POINT('Ctrl Pts',(-27.2643528843624,24.378143116702,-17.7360922397967));
#69722=CARTESIAN_POINT('Ctrl Pts',(-26.2543994639211,20.8730275468708,-17.537205328422));
#69723=CARTESIAN_POINT('Ctrl Pts',(-22.7595642866141,19.8280547468462,-17.3383184170471));
#69724=CARTESIAN_POINT('Ctrl Pts',(-19.9913045672277,22.203466120768,-17.1394315056721));
#69725=CARTESIAN_POINT('Ctrl Pts',(-20.4934162781595,25.8164600176741,-16.9405445942973));
#69726=CARTESIAN_POINT('Ctrl Pts',(-23.8045013291156,27.3470013776734,-16.7416576829224));
#69727=CARTESIAN_POINT('Ctrl Pts',(-26.8819532919847,25.3886524594344,-16.5427707715474));
#69728=CARTESIAN_POINT('Ctrl Pts',(-26.8978547377877,21.7409698782115,-16.3438838601725));
#69729=CARTESIAN_POINT('Ctrl Pts',(-23.8375935860521,19.7558646536676,-16.1449969487976));
#69730=CARTESIAN_POINT('Ctrl Pts',(-20.5132903678653,21.2574801779906,-15.9461100374227));
#69731=CARTESIAN_POINT('Ctrl Pts',(-19.9796978863084,24.865959100329,-15.7472231260478));
#69732=CARTESIAN_POINT('Ctrl Pts',(-22.7271423907501,27.2654152396129,-15.5483362146729));
#69733=CARTESIAN_POINT('Ctrl Pts',(-26.2309553264881,26.2509518441721,-15.3494493032982));
#69734=CARTESIAN_POINT('Ctrl Pts',(-27.2714296799262,22.754774762105,-15.1505623919233));
#69735=CARTESIAN_POINT('Ctrl Pts',(-24.8924577379321,19.9895743048977,-14.9516754805484));
#69736=CARTESIAN_POINT('Ctrl Pts',(-21.2801130116403,20.4963352423877,-14.7527885691735));
#69737=CARTESIAN_POINT('Ctrl Pts',(-19.7538340281876,23.8093872392638,-14.5539016577985));
#69738=CARTESIAN_POINT('Ctrl Pts',(-21.7161417662494,26.8843164108834,-14.3550147464236));
#69739=CARTESIAN_POINT('Ctrl Pts',(-25.3638417908065,26.8955235595285,-14.1561278350487));
#69740=CARTESIAN_POINT('Ctrl Pts',(-27.3450070532511,23.8327102658038,-13.9572409236738));
#69741=CARTESIAN_POINT('Ctrl Pts',(-25.8391146525105,20.5103422628989,-13.758354012299));
#69742=CARTESIAN_POINT('Ctrl Pts',(-22.2299520262449,19.9813940551297,-13.559467100924));
#69743=CARTESIAN_POINT('Ctrl Pts',(-19.8340336214646,22.7319241980239,-13.3605801895492));
#69744=CARTESIAN_POINT('Ctrl Pts',(-20.8530053117815,26.2344286967601,-13.1616932781742));
#69745=CARTESIAN_POINT('Ctrl Pts',(-24.3505185083463,27.2704028804096,-12.9628063667995));
#69746=CARTESIAN_POINT('Ctrl Pts',(-27.1126551237336,24.8878743103246,-12.7639194554245));
#69747=CARTESIAN_POINT('Ctrl Pts',(-26.6012457989672,21.2761847373024,-12.5650325440497));
#69748=CARTESIAN_POINT('Ctrl Pts',(-23.2862323431474,19.7541706581732,-12.3661456326747));
#69749=CARTESIAN_POINT('Ctrl Pts',(-20.2138310553815,21.7204339661432,-12.1672587212998));
#69750=CARTESIAN_POINT('Ctrl Pts',(-20.2073182224554,25.3681453928246,-11.9683718099249));
#69751=CARTESIAN_POINT('Ctrl Pts',(-23.2726785856307,27.345367412024,-11.76948489855));
#69752=CARTESIAN_POINT('Ctrl Pts',(-26.5931058708488,25.8352006288795,-11.5705979871751));
#69753=CARTESIAN_POINT('Ctrl Pts',(-27.1174089288021,22.2253602760722,-11.3717110758003));
#69754=CARTESIAN_POINT('Ctrl Pts',(-24.3637977028,19.8329835738428,-11.1728241644253));
#69755=CARTESIAN_POINT('Ctrl Pts',(-20.8626074418074,20.8564618714457,-10.9739372530505));
#69756=CARTESIAN_POINT('Ctrl Pts',(-19.8311351436954,24.3553053900332,-10.7750503416756));
#69757=CARTESIAN_POINT('Ctrl Pts',(-22.217216396,27.1143735890334,-10.5761634303007));
#69758=CARTESIAN_POINT('Ctrl Pts',(-25.8282448341817,26.5983167239714,-10.3772765189258));
#69759=CARTESIAN_POINT('Ctrl Pts',(-27.3459914882739,23.2813472994325,-10.1783896075509));
#69760=CARTESIAN_POINT('Ctrl Pts',(-25.3757758668614,20.2114789839381,-9.97950269617605));
#69761=CARTESIAN_POINT('Ctrl Pts',(-21.7280590792846,20.2096604775172,-9.78061578480118));
#69762=CARTESIAN_POINT('Ctrl Pts',(-19.7547835779453,23.2775628333863,-9.58172887342627));
#69763=CARTESIAN_POINT('Ctrl Pts',(-21.2692222424017,26.5960439017268,-9.3828419620514));
#69764=CARTESIAN_POINT('Ctrl Pts',(-24.8797343432425,27.1157009415294,-9.18395505067649));
#69765=CARTESIAN_POINT('Ctrl Pts',(-27.2685653807394,24.3590131928669,-8.98506813930161));
#69766=CARTESIAN_POINT('Ctrl Pts',(-26.2405821709042,20.8591429681827,-8.78618122792672));
#69767=CARTESIAN_POINT('Ctrl Pts',(-22.7404141249726,19.8321742639014,-8.58729431655183));
#69768=CARTESIAN_POINT('Ctrl Pts',(-19.9844189118443,22.2218042466703,-8.38840740517693));
#69769=CARTESIAN_POINT('Ctrl Pts',(-20.5051224625242,25.8321655695358,-8.18952049380205));
#69770=CARTESIAN_POINT('Ctrl Pts',(-23.8240423623182,27.345642284945,-7.99063358242715));
#69771=CARTESIAN_POINT('Ctrl Pts',(-26.8913726213182,25.3714776131012,-7.79174667105227));
#69772=CARTESIAN_POINT('Ctrl Pts',(-26.8884967982223,21.7237615058669,-7.59285975967737));
#69773=CARTESIAN_POINT('Ctrl Pts',(-23.8180575306258,19.7544357904668,-7.39397284830249));
#69774=CARTESIAN_POINT('Ctrl Pts',(-20.5015281751307,21.2731438280677,-7.19508593692757));
#69775=CARTESIAN_POINT('Ctrl Pts',(-19.9865180141189,24.8843216973216,-6.99619902555271));
#69776=CARTESIAN_POINT('Ctrl Pts',(-22.7462777198995,27.2696031137762,-6.7973121141778));
#69777=CARTESIAN_POINT('Ctrl Pts',(-26.2448221118963,26.2371166942234,-6.59842520280293));
#69778=CARTESIAN_POINT('Ctrl Pts',(-27.2672855215128,22.7356299178198,-6.39953829142803));
#69779=CARTESIAN_POINT('Ctrl Pts',(-24.8741107659123,19.9827122549589,-6.20065138005315));
#69780=CARTESIAN_POINT('Ctrl Pts',(-21.2644225377335,20.5080616288833,-6.00176446867825));
#69781=CARTESIAN_POINT('Ctrl Pts',(-19.7552182675814,23.8289265072379,-5.80287755730336));
#69782=CARTESIAN_POINT('Ctrl Pts',(-21.7333287203051,26.8937136297246,-5.60399064592847));
#69783=CARTESIAN_POINT('Ctrl Pts',(-25.38103810596,26.8861434818744,-5.40510373455358));
#69784=CARTESIAN_POINT('Ctrl Pts',(-27.3464107738837,23.8131723877192,-5.20621682317869));
#69785=CARTESIAN_POINT('Ctrl Pts',(-25.8234358783764,20.4986002378046,-5.0073299118038));
#69786=CARTESIAN_POINT('Ctrl Pts',(-22.2115982214328,19.9882378085279,-4.8084430004289));
#69787=CARTESIAN_POINT('Ctrl Pts',(-19.8298703764505,22.7510649007961,-4.60955608905403));
#69788=CARTESIAN_POINT('Ctrl Pts',(-20.8668582957487,26.2482776659228,-4.41066917767912));
#69789=CARTESIAN_POINT('Ctrl Pts',(-24.3696580035682,27.2662340875012,-4.21178226630423));
#69790=CARTESIAN_POINT('Ctrl Pts',(-27.1194935568628,24.8695185225726,-4.01289535492935));
#69791=CARTESIAN_POINT('Ctrl Pts',(-26.5894992297616,21.2605093673368,-3.81400844355446));
#69792=CARTESIAN_POINT('Ctrl Pts',(-23.266694872762,19.7555800419401,-3.61512153217957));
#69793=CARTESIAN_POINT('Ctrl Pts',(-20.2044559625963,21.737632999457,-3.41623462080468));
#69794=CARTESIAN_POINT('Ctrl Pts',(-20.2167204226629,25.3853296223073,-3.21734770942979));
#69795=CARTESIAN_POINT('Ctrl Pts',(-23.2922182540157,27.3467459877636,-3.0184607980549));
#69796=CARTESIAN_POINT('Ctrl Pts',(-26.6048277088558,25.819506756655,-2.81957388668));
#69797=CARTESIAN_POINT('Ctrl Pts',(-27.1105415611508,22.2070152938372,-2.62068697530512));
#69798=CARTESIAN_POINT('Ctrl Pts',(-24.3446516581053,19.8288449648733,-2.42180006393022));
#69799=CARTESIAN_POINT('Ctrl Pts',(-20.8487763118266,20.8703326664884,-2.22291315255534));
#69800=CARTESIAN_POINT('Ctrl Pts',(-19.8353285641946,24.3744395044934,-2.02402624118044));
#69801=CARTESIAN_POINT('Ctrl Pts',(-22.2355809690839,27.1211883940276,-1.82513932980556));
#69802=CARTESIAN_POINT('Ctrl Pts',(-25.8439050742452,26.58654999151,-1.62625241843066));
#69803=CARTESIAN_POINT('Ctrl Pts',(-27.3445569624681,23.2618116589932,-1.42736550705577));
#69804=CARTESIAN_POINT('Ctrl Pts',(-25.3585647827739,20.2021260327354,-1.22847859568088));
#69805=CARTESIAN_POINT('Ctrl Pts',(-21.7108869639328,20.2190847847069,-1.02959168430599));
#69806=CARTESIAN_POINT('Ctrl Pts',(-19.753430149382,23.2971042597106,-0.830704772931089));
#69807=CARTESIAN_POINT('Ctrl Pts',(-21.2849311867248,26.6077455332334,-0.631817861556202));
#69808=CARTESIAN_POINT('Ctrl Pts',(-24.8980704725179,27.1088099709984,-0.432930950181307));
#69809=CARTESIAN_POINT('Ctrl Pts',(-27.2726793468103,24.3398618379586,-0.234044038806425));
#69810=CARTESIAN_POINT('Ctrl Pts',(-26.2266935877583,20.8453297002904,-0.0351571274315334));
#69811=CARTESIAN_POINT('Ctrl Pts',(-22.7212854229633,19.8363923050463,0.163729783943363));
#69812=CARTESIAN_POINT('Ctrl Pts',(-19.9776277462716,22.2401775746711,0.362616695318246));
#69813=CARTESIAN_POINT('Ctrl Pts',(-20.5169093387535,25.8478106537611,0.56150360669314));
#69814=CARTESIAN_POINT('Ctrl Pts',(-23.843576140457,27.3441826194761,0.760390518068034));
#69815=CARTESIAN_POINT('Ctrl Pts',(-26.9007034154483,25.3542545067447,0.959277429442919));
#69816=CARTESIAN_POINT('Ctrl Pts',(-26.8790503996589,21.706601533086,1.15816434081781));
#69817=CARTESIAN_POINT('Ctrl Pts',(-23.7985143787261,19.7531075113212,1.3570512521927));
#69818=CARTESIAN_POINT('Ctrl Pts',(-20.4898467695046,21.2888678184727,1.55593816356758));
#69819=CARTESIAN_POINT('Ctrl Pts',(-19.9934325761168,24.9026489432696,1.75482507494249));
#69820=CARTESIAN_POINT('Ctrl Pts',(-22.7654343533035,27.2736924301352,1.95371198631737));
#69821=CARTESIAN_POINT('Ctrl Pts',(-26.258617494823,26.2232103459762,2.15259889769227));
#69822=CARTESIAN_POINT('Ctrl Pts',(-27.2630428667078,22.7165066599418,2.35148580906715));
#69823=CARTESIAN_POINT('Ctrl Pts',(-24.8557287134238,19.9759447400551,2.55037272044204));
#69824=CARTESIAN_POINT('Ctrl Pts',(-21.2487926352574,20.5198686293597,2.74925963181693));
#69825=CARTESIAN_POINT('Ctrl Pts',(-19.756703070296,23.8484583907251,2.94814654319182));
#69826=CARTESIAN_POINT('Ctrl Pts',(-21.7505638204061,26.9030222513286,3.14703345456672));
#69827=CARTESIAN_POINT('Ctrl Pts',(-25.3981859077504,26.8766750075821,3.34592036594163));
#69828=CARTESIAN_POINT('Ctrl Pts',(-27.3477139014116,23.7936275426109,3.5448072773165));
#69829=CARTESIAN_POINT('Ctrl Pts',(-25.807696867931,20.4869390774053,3.74369418869139));
#69830=CARTESIAN_POINT('Ctrl Pts',(-22.193279889165,19.9951759505411,3.94258110006629));
#69831=CARTESIAN_POINT('Ctrl Pts',(-19.8258057165764,22.7702267809692,4.14146801144116));
#69832=CARTESIAN_POINT('Ctrl Pts',(-20.8807823860657,26.2620551410361,4.34035492281606));
#69833=CARTESIAN_POINT('Ctrl Pts',(-24.3887757856436,27.2619668260629,4.53924183419096));
#69834=CARTESIAN_POINT('Ctrl Pts',(-27.1262374098896,24.8511277760402,4.73812874556585));
#69835=CARTESIAN_POINT('Ctrl Pts',(-26.5776721245927,21.2448946724955,4.93701565694073));
#69836=CARTESIAN_POINT('Ctrl Pts',(-23.2471649162744,19.7570899794412,5.13590256831564));
#69837=CARTESIAN_POINT('Ctrl Pts',(-20.1951695289349,21.7548800647585,5.3347894796905));
#69838=CARTESIAN_POINT('Ctrl Pts',(-20.2262109570028,25.4024652247072,5.53367639106541));
#69839=CARTESIAN_POINT('Ctrl Pts',(-23.3117647599631,27.3480239615159,5.73256330244029));
#69840=CARTESIAN_POINT('Ctrl Pts',(-26.6164686047155,25.8037527522356,5.9314502138152));
#69841=CARTESIAN_POINT('Ctrl Pts',(-27.103579850613,22.1887059055884,6.13033712519007));
#69842=CARTESIAN_POINT('Ctrl Pts',(-24.3254845628985,19.8248049682154,6.32922403656497));
#69843=CARTESIAN_POINT('Ctrl Pts',(-20.8350167673442,20.8842744758149,6.52811094793986));
#69844=CARTESIAN_POINT('Ctrl Pts',(-19.839620425199,24.3935517791038,6.72699785931474));
#69845=CARTESIAN_POINT('Ctrl Pts',(-22.2539803792018,27.1279085740085,6.92588477068964));
#69846=CARTESIAN_POINT('Ctrl Pts',(-25.859504535591,26.5747028012364,7.12477168206453));
#69847=CARTESIAN_POINT('Ctrl Pts',(-27.3430218926811,23.2422836618503,7.32365859343941));
#69848=CARTESIAN_POINT('Ctrl Pts',(-25.3413057808361,20.1928618023966,7.52254550481432));
#69849=CARTESIAN_POINT('Ctrl Pts',(-21.6937635893028,20.2285973633762,7.7214324161892));
#69850=CARTESIAN_POINT('Ctrl Pts',(-19.7521773315221,23.3166523941248,7.92031932756408));
#69851=CARTESIAN_POINT('Ctrl Pts',(-21.3007001590269,26.6193661452741,8.11920623893899));
#69852=CARTESIAN_POINT('Ctrl Pts',(-24.9163708864247,27.101824703466,8.31809315031388));
#69853=CARTESIAN_POINT('Ctrl Pts',(-27.2766946735608,24.3206895594619,8.51698006168875));
#69854=CARTESIAN_POINT('Ctrl Pts',(-26.2127340825124,20.8315881092272,8.71586697306367));
#69855=CARTESIAN_POINT('Ctrl Pts',(-22.7021786874711,19.8407087585086,8.91475388443853));
#69856=CARTESIAN_POINT('Ctrl Pts',(-19.9709312504664,22.258585617902,9.11364079581345));
#69857=CARTESIAN_POINT('Ctrl Pts',(-20.5287765945112,25.863394855776,9.31252770718832));
#69858=CARTESIAN_POINT('Ctrl Pts',(-23.8631021459136,27.3426224199458,9.51141461856321));
#69859=CARTESIAN_POINT('Ctrl Pts',(-26.9099454271214,25.3369835967543,9.71030152993811));
#69860=CARTESIAN_POINT('Ctrl Pts',(-26.8695157924143,21.6894904145851,9.909188441313));
#69861=CARTESIAN_POINT('Ctrl Pts',(-23.7789646482203,19.7518798514284,10.1080753526879));
#69862=CARTESIAN_POINT('Ctrl Pts',(-20.4782464605285,21.3046517325413,10.3069622640628));
#69863=CARTESIAN_POINT('Ctrl Pts',(-20.0004413890756,24.9209403525256,10.5058491754377));
#69864=CARTESIAN_POINT('Ctrl Pts',(-22.7846117833373,27.2776830803283,10.7047360868126));
#69865=CARTESIAN_POINT('Ctrl Pts',(-26.2723411097087,26.2092331679301,10.9036229981875));
#69866=CARTESIAN_POINT('Ctrl Pts',(-27.2587018279362,22.6974054952116,11.1025099095624));
#69867=CARTESIAN_POINT('Ctrl Pts',(-24.8373120675665,19.9692719395162,11.3013968209372));
#69868=CARTESIAN_POINT('Ctrl Pts',(-21.2332237183833,20.5317559309471,11.5002837323122));
#69869=CARTESIAN_POINT('Ctrl Pts',(-19.7582883969858,23.8679823721571,11.699170643687));
#69870=CARTESIAN_POINT('Ctrl Pts',(-21.7678466098456,26.9122420290296,11.8980575550619));
#69871=CARTESIAN_POINT('Ctrl Pts',(-25.4152847417835,26.8671183875534,12.0969444664368));
#69872=CARTESIAN_POINT('Ctrl Pts',(-27.3489164013039,23.774076248391,12.2958313778117));
#69873=CARTESIAN_POINT('Ctrl Pts',(-25.7918980382369,20.475359090706,12.4947182891866));
#69874=CARTESIAN_POINT('Ctrl Pts',(-22.1749975148535,20.0022082973181,12.6936052005615));
#69875=CARTESIAN_POINT('Ctrl Pts',(-19.82183974955,22.7894093307791,12.8924921119364));
#69876=CARTESIAN_POINT('Ctrl Pts',(-20.8947772137633,26.2757607570156,13.0913790233113));
#69877=CARTESIAN_POINT('Ctrl Pts',(-24.4078713479767,27.2576012091716,13.2902659346862));
#69878=CARTESIAN_POINT('Ctrl Pts',(-27.132886504111,24.8327025580578,13.4891528460611));
#69879=CARTESIAN_POINT('Ctrl Pts',(-26.565764796863,21.2293410665471,13.6880397574359));
#69880=CARTESIAN_POINT('Ctrl Pts',(-23.2276429912025,19.7587004306651,13.8869266688109));
#69881=CARTESIAN_POINT('Ctrl Pts',(-20.1859720004754,21.7721747050237,14.0858135801857));
#69882=CARTESIAN_POINT('Ctrl Pts',(-20.2357895739884,25.4195517459537,14.2847004915607));
#69883=CARTESIAN_POINT('Ctrl Pts',(-23.3313175855166,27.3492012994163,14.4835874029355));
#69884=CARTESIAN_POINT('Ctrl Pts',(-26.6280282499597,25.7879390330813,14.6824743143104));
#69885=CARTESIAN_POINT('Ctrl Pts',(-27.0965239816645,22.1704325964997,14.8813612256853));
#69886=CARTESIAN_POINT('Ctrl Pts',(-24.306296925082,19.820863690924,15.0802481370602));
#69887=CARTESIAN_POINT('Ctrl Pts',(-20.8213291729697,20.8982869299861,15.2791350484351));
#69888=CARTESIAN_POINT('Ctrl Pts',(-19.8440106129798,24.4126417074145,15.47802195981));
#69889=CARTESIAN_POINT('Ctrl Pts',(-22.272414138794,27.1345339509001,15.6769088711849));
#69890=CARTESIAN_POINT('Ctrl Pts',(-25.8750428048544,26.5627754670849,15.8757957825598));
#69891=CARTESIAN_POINT('Ctrl Pts',(-27.3413863195906,23.2227638254696,16.0746826939346));
#69892=CARTESIAN_POINT('Ctrl Pts',(-25.3239993183881,20.1836865384115,16.2735696053096));
#69893=CARTESIAN_POINT('Ctrl Pts',(-21.676689409141,20.2381979614547,16.4724565166844));
#69894=CARTESIAN_POINT('Ctrl Pts',(-19.7510251575634,23.3362067186294,16.6713434280593));
#69895=CARTESIAN_POINT('Ctrl Pts',(-21.3165287414511,26.6309054299184,16.8702303394342));
#69896=CARTESIAN_POINT('Ctrl Pts',(-24.9346351000264,27.0947453240317,17.0691172508091));
#69897=CARTESIAN_POINT('Ctrl Pts',(-27.2806112545899,24.301496865417,17.268004162184));
#69898=CARTESIAN_POINT('Ctrl Pts',(-26.1987040250745,20.8179185591267,17.4668910735589));
#69899=CARTESIAN_POINT('Ctrl Pts',(-22.6830944247988,19.8451235099081,17.6657779849338));
#69900=CARTESIAN_POINT('Ctrl Pts',(-19.964329601877,22.2770278885748,17.8646648963087));
#69901=CARTESIAN_POINT('Ctrl Pts',(-20.5407239153308,25.8789177626204,18.0635518076836));
#69902=CARTESIAN_POINT('Ctrl Pts',(-23.8826198612747,27.3409617276973,18.2624387190584));
#69903=CARTESIAN_POINT('Ctrl Pts',(-26.9190984114366,25.3196653407859,18.4613256304333));
#69904=CARTESIAN_POINT('Ctrl Pts',(-26.8598932291429,21.6724286037856,18.6602125418082));
#69905=CARTESIAN_POINT('Ctrl Pts',(-23.7594088571501,19.7507528433199,18.8590994531831));
#69906=CARTESIAN_POINT('Ctrl Pts',(-20.4667275555952,21.3204951520206,19.057986364558));
#69907=CARTESIAN_POINT('Ctrl Pts',(-20.0075442672708,24.9391954403919,19.2568732759329));
#69908=CARTESIAN_POINT('Ctrl Pts',(-22.8038095018245,27.2815749586085,19.4557601873078));
#69909=CARTESIAN_POINT('Ctrl Pts',(-26.2859925928962,26.1951855304619,19.6546470986827));
#69910=CARTESIAN_POINT('Ctrl Pts',(-27.2542625202295,22.6783269297847,19.8535340100576));
#69911=CARTESIAN_POINT('Ctrl Pts',(-24.818861316357,19.9626940301626,20.0524209214325));
#69912=CARTESIAN_POINT('Ctrl Pts',(-21.2177161996666,20.5437232186478,20.2513078328074));
#69913=CARTESIAN_POINT('Ctrl Pts',(-19.7599742056419,23.887497934174,20.4501947441822));
#69914=CARTESIAN_POINT('Ctrl Pts',(-21.7851766306525,26.9213727185159,20.6490816555571));
#69915=CARTESIAN_POINT('Ctrl Pts',(-25.4323341549631,26.857473875026,20.847968566932));
#69916=CARTESIAN_POINT('Ctrl Pts',(-27.3500182416961,23.7545190231427,21.0468554783069));
#69917=CARTESIAN_POINT('Ctrl Pts',(-25.7760398079417,20.4638605845609,21.2457423896818));
#69918=CARTESIAN_POINT('Ctrl Pts',(-22.1567515829562,20.0093346625109,21.4446293010567));
#69919=CARTESIAN_POINT('Ctrl Pts',(-19.8179725804642,22.8086120419138,21.6435162124316));
#69920=CARTESIAN_POINT('Ctrl Pts',(-20.908842407997,26.2893941506808,21.8424031238065));
#69921=CARTESIAN_POINT('Ctrl Pts',(-24.426944184561,27.2531373525101,22.0412900351814));
#69922=CARTESIAN_POINT('Ctrl Pts',(-27.1394406633346,24.8142433568688,22.2401769465563));
#69923=CARTESIAN_POINT('Ctrl Pts',(-26.5537775621008,21.2138489616415,22.4390638579311));
#69924=CARTESIAN_POINT('Ctrl Pts',(-23.2081296148507,19.7604113529361,22.637950769306));
#69925=CARTESIAN_POINT('Ctrl Pts',(-20.1768636209402,21.7895164619687,22.8368376806809));
#69926=CARTESIAN_POINT('Ctrl Pts',(-20.2454560197989,25.4365887332747,23.0357245920558));
#69927=CARTESIAN_POINT('Ctrl Pts',(-23.3508762125534,27.350277970271,23.2346115034307));
#69928=CARTESIAN_POINT('Ctrl Pts',(-26.639506338272,25.7720660182269,23.4334984148056));
#69929=CARTESIAN_POINT('Ctrl Pts',(-27.0893741412788,22.152195850804,23.6323853261805));
#69930=CARTESIAN_POINT('Ctrl Pts',(-24.2870892530986,19.8170212374106,23.8312722375554));
#69931=CARTESIAN_POINT('Ctrl Pts',(-20.8077138914136,20.9123696577412,24.0301591489302));
#69932=CARTESIAN_POINT('Ctrl Pts',(-19.8484990111886,24.431708783473,24.2290460603052));
#69933=CARTESIAN_POINT('Ctrl Pts',(-22.2908817594182,27.141064349319,24.42793297168));
#69934=CARTESIAN_POINT('Ctrl Pts',(-25.8905194702402,26.5507683047743,24.6268198830549));
#69935=CARTESIAN_POINT('Ctrl Pts',(-27.3396502866349,23.2032526677418,24.8257067944298));
#69936=CARTESIAN_POINT('Ctrl Pts',(-25.3066458538429,20.174600482701,25.0245937058047));
#69937=CARTESIAN_POINT('Ctrl Pts',(-21.6596648762396,20.2478863268259,25.2234806171796));
#69938=CARTESIAN_POINT('Ctrl Pts',(-19.7499736573778,23.3557667107438,25.4223675285545));
#69939=CARTESIAN_POINT('Ctrl Pts',(-21.3324165158066,26.6423630895425,25.6212544399294));
#69940=CARTESIAN_POINT('Ctrl Pts',(-24.9528626269947,27.0875720048975,25.8201413513043));
#69941=CARTESIAN_POINT('Ctrl Pts',(-27.2844289905532,24.2822842934685,26.0190282626791));
#69942=CARTESIAN_POINT('Ctrl Pts',(-26.1846037788393,20.8043213573341,26.2179151740541));
#69943=CARTESIAN_POINT('Ctrl Pts',(-22.6640331564827,19.8496365458834,26.416802085429));
#69944=CARTESIAN_POINT('Ctrl Pts',(-19.9578229455499,22.2955037023318,26.6156889968038));
#69945=CARTESIAN_POINT('Ctrl Pts',(-20.5527510410596,25.8943793324076,26.8145759081788));
#69946=CARTESIAN_POINT('Ctrl Pts',(-23.9021286627863,27.3391998891404,27.0134628195536));
#69947=CARTESIAN_POINT('Ctrl Pts',(-26.928162327061,25.3023015149534,27.2123497309286));
#69948=CARTESIAN_POINT('Ctrl Pts',(-26.8501825849064,21.6554140656546,27.4112366423034));
#69949=CARTESIAN_POINT('Ctrl Pts',(-23.7398482410897,19.7497312131016,27.6101235536783));
#69950=CARTESIAN_POINT('Ctrl Pts',(-20.4552890053948,21.3363887896213,27.8090104650532));
#69951=CARTESIAN_POINT('Ctrl Pts',(-20.0147435801427,24.9574304667042,28.0078973764281));
#69952=CARTESIAN_POINT('Ctrl Pts',(-22.8230221706751,27.285336346559,28.206784287803));
#69953=CARTESIAN_POINT('Ctrl Pts',(-26.2995807014884,26.1811275020712,28.4056711991778));
#69954=CARTESIAN_POINT('Ctrl Pts',(-27.2497078429493,22.6591587491998,28.6045581105528));
#69955=CARTESIAN_POINT('Ctrl Pts',(-24.8004094605876,19.9564240356054,28.8034450219277));
#69956=CARTESIAN_POINT('Ctrl Pts',(-21.2022090988071,20.5553681827278,29.0023319333025));
#69957=CARTESIAN_POINT('Ctrl Pts',(-19.7618763887169,23.9077643379941,29.2012188446774));
#69958=CARTESIAN_POINT('Ctrl Pts',(-21.8023343633778,26.9289734564946,29.4001057560523));
#69959=CARTESIAN_POINT('Ctrl Pts',(-25.4497485501313,26.8505109829531,29.5989926674272));
#69960=CARTESIAN_POINT('Ctrl Pts',(-27.3506339076343,23.7286560066104,29.797922464558));
#69961=CARTESIAN_POINT('Ctrl Pts',(-26.290666056329,21.5524040433688,29.9305566245639));
#69962=CARTESIAN_POINT('Ctrl Pts',(-25.4168923872279,20.930003392908,29.9968951474449));
#69963=CARTESIAN_POINT('Ctrl Pts',(-25.087202831673,26.6465417208825,-75.274954513805));
#69964=CARTESIAN_POINT('Ctrl Pts',(-26.1190047250109,26.1343711410084,-75.2086588766801));
#69965=CARTESIAN_POINT('Ctrl Pts',(-27.6122618789375,24.0062782296181,-75.0760676024301));
#69966=CARTESIAN_POINT('Ctrl Pts',(-26.1265778059314,20.3717807620434,-74.8771806910553));
#69967=CARTESIAN_POINT('Ctrl Pts',(-22.2702066924084,19.668455682932,-74.6782937796803));
#69968=CARTESIAN_POINT('Ctrl Pts',(-19.5917683008039,22.526906813967,-74.4794068683055));
#69969=CARTESIAN_POINT('Ctrl Pts',(-20.5499578780943,26.3284832670958,-74.2805199569306));
#69970=CARTESIAN_POINT('Ctrl Pts',(-24.2656310039462,27.5756447695868,-74.0816330455557));
#69971=CARTESIAN_POINT('Ctrl Pts',(-27.3236846535468,25.1245829777789,-73.8827461341808));
#69972=CARTESIAN_POINT('Ctrl Pts',(-26.9144050854087,21.2264367862693,-73.6838592228059));
#69973=CARTESIAN_POINT('Ctrl Pts',(-23.4136851936635,19.4638964155144,-73.484972311431));
#69974=CARTESIAN_POINT('Ctrl Pts',(-20.0384958396557,21.4562563619107,-73.2860854000561));
#69975=CARTESIAN_POINT('Ctrl Pts',(-19.8902936837951,25.3728818798044,-73.0871984886812));
#69976=CARTESIAN_POINT('Ctrl Pts',(-23.1052936987138,27.6146334487714,-72.8883115773064));
#69977=CARTESIAN_POINT('Ctrl Pts',(-26.7291676983987,26.1215805639939,-72.6894246659315));
#69978=CARTESIAN_POINT('Ctrl Pts',(-27.4318910772013,22.2656862235542,-72.4905377545565));
#69979=CARTESIAN_POINT('Ctrl Pts',(-24.5677162109303,19.5902041769872,-72.2916508431817));
#69980=CARTESIAN_POINT('Ctrl Pts',(-20.7685793006563,20.5536682854776,-72.0927639318068));
#69981=CARTESIAN_POINT('Ctrl Pts',(-19.5255638134539,24.2707405856734,-71.8938770204319));
#69982=CARTESIAN_POINT('Ctrl Pts',(-21.980896248319,27.3257447430297,-71.694990109057));
#69983=CARTESIAN_POINT('Ctrl Pts',(-25.878333927738,26.9113920423683,-71.4961031976822));
#69984=CARTESIAN_POINT('Ctrl Pts',(-27.6364622567071,23.4084369102996,-71.2972162863072));
#69985=CARTESIAN_POINT('Ctrl Pts',(-25.6397102680719,20.0357984155606,-71.0983293749323));
#69986=CARTESIAN_POINT('Ctrl Pts',(-21.7229237943914,19.8926452212372,-70.8994424635574));
#69987=CARTESIAN_POINT('Ctrl Pts',(-19.4852974888931,23.1105230607847,-70.7005555521826));
#69988=CARTESIAN_POINT('Ctrl Pts',(-20.9830202213933,26.7324749855528,-70.5016686408076));
#69989=CARTESIAN_POINT('Ctrl Pts',(-24.8398117789982,27.4302342914755,-70.3027817294328));
#69990=CARTESIAN_POINT('Ctrl Pts',(-27.5116077263315,24.5626193239777,-70.1038948180579));
#69991=CARTESIAN_POINT('Ctrl Pts',(-26.5432541165811,20.764725111243,-69.905007906683));
#69992=CARTESIAN_POINT('Ctrl Pts',(-22.8245858154009,19.5264944228945,-69.7061209953081));
#69993=CARTESIAN_POINT('Ctrl Pts',(-19.7727436998939,21.9857562787565,-69.5072340839333));
#69994=CARTESIAN_POINT('Ctrl Pts',(-20.1921119209898,25.8826575433156,-69.3083471725583));
#69995=CARTESIAN_POINT('Ctrl Pts',(-23.6973266398938,27.6362763577108,-69.1094602611835));
#69996=CARTESIAN_POINT('Ctrl Pts',(-27.0673927232214,25.6351857135901,-68.9105733498085));
#69997=CARTESIAN_POINT('Ctrl Pts',(-27.205505174831,21.7182182485408,-68.7116864384336));
#69998=CARTESIAN_POINT('Ctrl Pts',(-23.9847503617234,19.4847349587904,-68.5127995270588));
#69999=CARTESIAN_POINT('Ctrl Pts',(-20.3647288821552,20.9871176195064,-68.3139126156839));
#70000=CARTESIAN_POINT('Ctrl Pts',(-19.67193354865,24.8448039465122,-68.115025704309));
#70001=CARTESIAN_POINT('Ctrl Pts',(-22.5429845333374,27.5129072831641,-67.916138792934));
#70002=CARTESIAN_POINT('Ctrl Pts',(-26.3396294062728,26.5396668809304,-67.7172518815593));
#70003=CARTESIAN_POINT('Ctrl Pts',(-27.5730734316282,22.819408152289,-67.5183649701843));
#70004=CARTESIAN_POINT('Ctrl Pts',(-25.1098861289101,19.7707334429356,-67.3194780588094));
#70005=CARTESIAN_POINT('Ctrl Pts',(-21.2135277854729,20.1951163257777,-67.1205911474346));
#70006=CARTESIAN_POINT('Ctrl Pts',(-19.4644213622264,23.7025849132179,-66.9217042360596));
#70007=CARTESIAN_POINT('Ctrl Pts',(-21.4698473623653,27.0700729576938,-66.7228173246848));
#70008=CARTESIAN_POINT('Ctrl Pts',(-25.386989323847,27.2031444622345,-66.5239304133098));
#70009=CARTESIAN_POINT('Ctrl Pts',(-27.6163259029392,23.97951799677,-66.325043501935));
#70010=CARTESIAN_POINT('Ctrl Pts',(-26.1092858000276,20.3614329646103,-66.1261565905601));
#70011=CARTESIAN_POINT('Ctrl Pts',(-22.2507110937587,19.6736027472872,-65.9272696791851));
#70012=CARTESIAN_POINT('Ctrl Pts',(-19.5863047860085,22.5480849961352,-65.7283827678104));
#70013=CARTESIAN_POINT('Ctrl Pts',(-20.5644303691982,26.3434742403671,-65.5294958564353));
#70014=CARTESIAN_POINT('Ctrl Pts',(-24.2862733637496,27.572129560475,-65.3306089450606));
#70015=CARTESIAN_POINT('Ctrl Pts',(-27.3317756179178,25.1050208900719,-65.1317220336856));
#70016=CARTESIAN_POINT('Ctrl Pts',(-26.9023787761313,21.2092119209378,-64.9328351223108));
#70017=CARTESIAN_POINT('Ctrl Pts',(-23.3926621291436,19.4646207855772,-64.7339482109358));
#70018=CARTESIAN_POINT('Ctrl Pts',(-20.0277577006371,21.4743788204509,-64.5350612995609));
#70019=CARTESIAN_POINT('Ctrl Pts',(-19.8997273635616,25.3916887908911,-64.3361743881861));
#70020=CARTESIAN_POINT('Ctrl Pts',(-23.1262201425069,27.6168749671773,-64.1372874768111));
#70021=CARTESIAN_POINT('Ctrl Pts',(-26.7423627350975,26.105179917978,-63.9384005654363));
#70022=CARTESIAN_POINT('Ctrl Pts',(-27.425226697074,22.2457232229035,-63.7395136540614));
#70023=CARTESIAN_POINT('Ctrl Pts',(-24.5473179446962,19.585018356762,-63.5406267426865));
#70024=CARTESIAN_POINT('Ctrl Pts',(-20.7531906149757,20.5680275009666,-63.3417398313116));
#70025=CARTESIAN_POINT('Ctrl Pts',(-19.5293260349772,24.2914485974244,-63.1428529199367));
#70026=CARTESIAN_POINT('Ctrl Pts',(-22.0003519871148,27.3337733525391,-62.9439660085619));
#70027=CARTESIAN_POINT('Ctrl Pts',(-25.8956051298252,26.8993632629622,-62.7450790971869));
#70028=CARTESIAN_POINT('Ctrl Pts',(-27.6356780879611,23.3874043691131,-62.546192185812));
#70029=CARTESIAN_POINT('Ctrl Pts',(-25.6215913468528,20.0250891294288,-62.3473052744372));
#70030=CARTESIAN_POINT('Ctrl Pts',(-21.7041198551841,19.9021001718582,-62.1484183630623));
#70031=CARTESIAN_POINT('Ctrl Pts',(-19.4830877669895,23.1314539206649,-61.9495314516874));
#70032=CARTESIAN_POINT('Ctrl Pts',(-20.9994352588532,26.7456480847409,-61.7506445403125));
#70033=CARTESIAN_POINT('Ctrl Pts',(-24.8597675508181,27.4235446604322,-61.5517576289376));
#70034=CARTESIAN_POINT('Ctrl Pts',(-27.5167665687724,24.5422141708298,-61.3528707175627));
#70035=CARTESIAN_POINT('Ctrl Pts',(-26.5288754915826,20.7493550393392,-61.1539838061878));
#70036=CARTESIAN_POINT('Ctrl Pts',(-22.8038824598357,19.5302832263775,-60.9550968948129));
#70037=CARTESIAN_POINT('Ctrl Pts',(-19.7647402423802,22.0052223678112,-60.7562099834381));
#70038=CARTESIAN_POINT('Ctrl Pts',(-20.2041628602908,25.8999132328981,-60.5573230720631));
#70039=CARTESIAN_POINT('Ctrl Pts',(-23.7183581846015,27.6354651319532,-60.3584361606884));
#70040=CARTESIAN_POINT('Ctrl Pts',(-27.0780786668995,25.6170530202798,-60.1595492493133));
#70041=CARTESIAN_POINT('Ctrl Pts',(-27.1960260412742,21.6994264953798,-59.9606623379385));
#70042=CARTESIAN_POINT('Ctrl Pts',(-23.9638166709638,19.4825521736829,-59.7617754265636));
#70043=CARTESIAN_POINT('Ctrl Pts',(-20.3515769211211,21.0035495968821,-59.5628885151886));
#70044=CARTESIAN_POINT('Ctrl Pts',(-19.6786488544269,24.8647510923725,-59.3640016038139));
#70045=CARTESIAN_POINT('Ctrl Pts',(-22.5633963092817,27.5180398616982,-59.1651146924389));
#70046=CARTESIAN_POINT('Ctrl Pts',(-26.354980960924,26.5252684876387,-58.9662277810641));
#70047=CARTESIAN_POINT('Ctrl Pts',(-27.5692579878596,22.7987096898228,-58.7673408696891));
#70048=CARTESIAN_POINT('Ctrl Pts',(-25.0904097560483,19.7627550433618,-58.5684539583142));
#70049=CARTESIAN_POINT('Ctrl Pts',(-21.1962876188541,20.2071894618475,-58.3695670469394));
#70050=CARTESIAN_POINT('Ctrl Pts',(-19.465259653248,23.7236153965165,-58.1706801355645));
#70051=CARTESIAN_POINT('Ctrl Pts',(-21.4879937926539,27.0807355571606,-57.9717932241896));
#70052=CARTESIAN_POINT('Ctrl Pts',(-25.4057688625309,27.1936411529989,-57.7729063128147));
#70053=CARTESIAN_POINT('Ctrl Pts',(-27.6184817462102,23.9585815142718,-57.5740194014398));
#70054=CARTESIAN_POINT('Ctrl Pts',(-26.0928369107051,20.3483021611443,-57.3751324900649));
#70055=CARTESIAN_POINT('Ctrl Pts',(-22.2307726064942,19.6803437179301,-57.17624557869));
#70056=CARTESIAN_POINT('Ctrl Pts',(-19.5811984800931,22.5685033604062,-56.9773586673151));
#70057=CARTESIAN_POINT('Ctrl Pts',(-20.5788485068248,26.358807252693,-56.7784717559402));
#70058=CARTESIAN_POINT('Ctrl Pts',(-24.3069668988959,27.5682874825533,-56.5795848445653));
#70059=CARTESIAN_POINT('Ctrl Pts',(-27.3397289463067,25.0855342657581,-56.3806979331904));
#70060=CARTESIAN_POINT('Ctrl Pts',(-26.8902834633044,21.1919873057831,-56.1818110218156));
#70061=CARTESIAN_POINT('Ctrl Pts',(-23.3716327420754,19.4654861405022,-55.9829241104406));
#70062=CARTESIAN_POINT('Ctrl Pts',(-20.0171184630454,21.4925389576496,-55.7840371990659));
#70063=CARTESIAN_POINT('Ctrl Pts',(-19.9092548327343,25.4104560840035,-55.5851502876908));
#70064=CARTESIAN_POINT('Ctrl Pts',(-23.1471593820707,27.6190038650373,-55.3862633763161));
#70065=CARTESIAN_POINT('Ctrl Pts',(-26.7554723592479,26.0887141439529,-55.187376464941));
#70066=CARTESIAN_POINT('Ctrl Pts',(-27.4184600727296,22.225793427255,-54.9884895535663));
#70067=CARTESIAN_POINT('Ctrl Pts',(-24.5268930259144,19.5799383319231,-54.7896026421912));
#70068=CARTESIAN_POINT('Ctrl Pts',(-20.7378761703695,20.582465359049,-54.5907157308165));
#70069=CARTESIAN_POINT('Ctrl Pts',(-19.5331947406888,24.3121371709789,-54.3918288194415));
#70070=CARTESIAN_POINT('Ctrl Pts',(-22.0198488306076,27.341701596571,-54.1929419080667));
#70071=CARTESIAN_POINT('Ctrl Pts',(-25.9128141649889,26.8872457934103,-53.9940549966918));
#70072=CARTESIAN_POINT('Ctrl Pts',(-27.6347856705658,23.3663761131036,-53.7951680853169));
#70073=CARTESIAN_POINT('Ctrl Pts',(-25.6034175328204,20.0144732713323,-53.596281173942));
#70074=CARTESIAN_POINT('Ctrl Pts',(-21.6853648387249,19.9116517851892,-53.3973942625671));
#70075=CARTESIAN_POINT('Ctrl Pts',(-19.4809858180664,23.1523958826153,-53.1985073511921));
#70076=CARTESIAN_POINT('Ctrl Pts',(-21.0159178903106,26.7587365078639,-52.9996204398173));
#70077=CARTESIAN_POINT('Ctrl Pts',(-24.8796886218434,27.416752393593,-52.8007335284424));
#70078=CARTESIAN_POINT('Ctrl Pts',(-27.5218203041215,24.5217827313643,-52.6018466170675));
#70079=CARTESIAN_POINT('Ctrl Pts',(-26.514417936956,20.734059187816,-52.4029597056927));
#70080=CARTESIAN_POINT('Ctrl Pts',(-22.7831988821365,19.5341785534718,-52.2040727943177));
#70081=CARTESIAN_POINT('Ctrl Pts',(-19.756837095836,22.024729398193,-52.0051858829429));
#70082=CARTESIAN_POINT('Ctrl Pts',(-20.2163024664992,25.9171066595697,-51.8062989715679));
#70083=CARTESIAN_POINT('Ctrl Pts',(-23.7393852747262,27.6345456535659,-51.6074120601931));
#70084=CARTESIAN_POINT('Ctrl Pts',(-27.0886711279188,25.5988655595124,-51.4085251488182));
#70085=CARTESIAN_POINT('Ctrl Pts',(-27.1864502996043,21.6806837866354,-51.2096382374433));
#70086=CARTESIAN_POINT('Ctrl Pts',(-23.9428720213101,19.4804771771778,-51.0107513260684));
#70087=CARTESIAN_POINT('Ctrl Pts',(-20.3385097207022,21.0200490584739,-50.8118644146935));
#70088=CARTESIAN_POINT('Ctrl Pts',(-19.6854667525116,24.8846634057819,-50.6129775033186));
#70089=CARTESIAN_POINT('Ctrl Pts',(-22.5838342355929,27.5230672991878,-50.4140905919437));
#70090=CARTESIAN_POINT('Ctrl Pts',(-26.370258194032,26.5107912604119,-50.2152036805689));
#70091=CARTESIAN_POINT('Ctrl Pts',(-27.5653360458338,22.7780311422346,-50.0163167691939));
#70092=CARTESIAN_POINT('Ctrl Pts',(-25.0708925710849,19.754877007394,-49.8174298578191));
#70093=CARTESIAN_POINT('Ctrl Pts',(-21.1791098291497,20.2193511846074,-49.618542946444));
#70094=CARTESIAN_POINT('Ctrl Pts',(-19.466206191105,23.7446412859314,-49.4196560350694));
#70095=CARTESIAN_POINT('Ctrl Pts',(-21.5061948700345,27.09130460356,-49.2207691236942));
#70096=CARTESIAN_POINT('Ctrl Pts',(-25.4244992325195,27.1840412988489,-49.0218822123197));
#70097=CARTESIAN_POINT('Ctrl Pts',(-27.6205297868606,23.9376342116029,-48.8229953009445));
#70098=CARTESIAN_POINT('Ctrl Pts',(-26.0763206463049,20.3352562050708,-48.6241083895698));
#70099=CARTESIAN_POINT('Ctrl Pts',(-22.2108690836787,19.6871872359689,-48.4252214781947));
#70100=CARTESIAN_POINT('Ctrl Pts',(-19.5761973487895,22.5889477397143,-48.22633456682));
#70101=CARTESIAN_POINT('Ctrl Pts',(-20.5933453826749,26.3740658420838,-48.0274476554451));
#70102=CARTESIAN_POINT('Ctrl Pts',(-24.327640382126,27.5643389320917,-47.8285607440701));
#70103=CARTESIAN_POINT('Ctrl Pts',(-27.3475818586505,25.0660069585364,-47.6296738326953));
#70104=CARTESIAN_POINT('Ctrl Pts',(-26.8780996441353,21.1748251814955,-47.4307869213203));
#70105=CARTESIAN_POINT('Ctrl Pts',(-23.3506080881922,19.4664597362608,-47.2319000099455));
#70106=CARTESIAN_POINT('Ctrl Pts',(-20.0065728487701,21.5107536214995,-47.0330130985705));
#70107=CARTESIAN_POINT('Ctrl Pts',(-19.9188787834653,25.4291740842155,-46.8341261871958));
#70108=CARTESIAN_POINT('Ctrl Pts',(-23.1681093030625,27.6210249464413,-46.6352392758207));
#70109=CARTESIAN_POINT('Ctrl Pts',(-26.7684970493695,26.072181104098,-46.436352364446));
#70110=CARTESIAN_POINT('Ctrl Pts',(-27.4115909460707,22.2058987279973,-46.237465453071));
#70111=CARTESIAN_POINT('Ctrl Pts',(-24.5064422274687,19.574963515088,-46.0385785416961));
#70112=CARTESIAN_POINT('Ctrl Pts',(-20.7226362499667,20.5969818595133,-45.8396916303212));
#70113=CARTESIAN_POINT('Ctrl Pts',(-19.5371698930469,24.332805555612,-45.6408047189464));
#70114=CARTESIAN_POINT('Ctrl Pts',(-22.0393862277468,27.3495293722852,-45.4419178075714));
#70115=CARTESIAN_POINT('Ctrl Pts',(-25.9299605954365,26.8750398980102,-45.2430308961966));
#70116=CARTESIAN_POINT('Ctrl Pts',(-27.633785018518,23.3453527295727,-45.0441439848217));
#70117=CARTESIAN_POINT('Ctrl Pts',(-25.5851893126678,20.0039511066464,-44.8452570734468));
#70118=CARTESIAN_POINT('Ctrl Pts',(-21.6666592392896,19.9212998165622,-44.6463701620719));
#70119=CARTESIAN_POINT('Ctrl Pts',(-19.4789916992562,23.1733483872337,-44.447483250697));
#70120=CARTESIAN_POINT('Ctrl Pts',(-21.0324676782386,26.7717399104627,-44.2485963393221));
#70121=CARTESIAN_POINT('Ctrl Pts',(-24.8995744645946,27.4098576696907,-44.0497094279473));
#70122=CARTESIAN_POINT('Ctrl Pts',(-27.5267687982487,24.501325547651,-43.8508225165723));
#70123=CARTESIAN_POINT('Ctrl Pts',(-26.4998818359196,20.718837961641,-43.6519356051975));
#70124=CARTESIAN_POINT('Ctrl Pts',(-22.7625356303309,19.5381803011428,-43.4530486938226));
#70125=CARTESIAN_POINT('Ctrl Pts',(-19.7490344697155,22.0442768528926,-43.2541617824477));
#70126=CARTESIAN_POINT('Ctrl Pts',(-20.2285304179152,25.9342373677798,-43.0552748710728));
#70127=CARTESIAN_POINT('Ctrl Pts',(-23.7604073530864,27.6335179468858,-42.8563879596979));
#70128=CARTESIAN_POINT('Ctrl Pts',(-27.0991698255887,25.5806238132462,-42.657501048323));
#70129=CARTESIAN_POINT('Ctrl Pts',(-27.1767782035679,21.6619906189565,-42.4586141369482));
#70130=CARTESIAN_POINT('Ctrl Pts',(-23.9219169677665,19.478510024264,-42.2597272255731));
#70131=CARTESIAN_POINT('Ctrl Pts',(-20.3255276271621,21.0366155670659,-42.0608403141984));
#70132=CARTESIAN_POINT('Ctrl Pts',(-19.6923870622387,24.9045403590919,-41.8619534028234));
#70133=CARTESIAN_POINT('Ctrl Pts',(-22.6042977706932,27.5279894624118,-41.6630664914486));
#70134=CARTESIAN_POINT('Ctrl Pts',(-26.3854607007702,26.4962355828775,-41.4641795800736));
#70135=CARTESIAN_POINT('Ctrl Pts',(-27.5613077094774,22.7573730574781,-41.2652926686988));
#70136=CARTESIAN_POINT('Ctrl Pts',(-25.0513350911988,19.7470995437899,-41.0664057573238));
#70137=CARTESIAN_POINT('Ctrl Pts',(-21.1619948715485,20.2316011717875,-40.867518845949));
#70138=CARTESIAN_POINT('Ctrl Pts',(-19.4672609507149,23.7656620243051,-40.668631934574));
#70139=CARTESIAN_POINT('Ctrl Pts',(-21.524450112203,27.1017798168263,-40.4697450231992));
#70140=CARTESIAN_POINT('Ctrl Pts',(-25.4431799374829,27.1743451541679,-40.2708581118243));
#70141=CARTESIAN_POINT('Ctrl Pts',(-27.6224699706203,23.9166766438388,-40.0719712004494));
#70142=CARTESIAN_POINT('Ctrl Pts',(-26.059737444486,20.3222954420901,-39.8730842890745));
#70143=CARTESIAN_POINT('Ctrl Pts',(-22.1910010527294,19.6941331200593,-39.6741973776996));
#70144=CARTESIAN_POINT('Ctrl Pts',(-19.5713015246209,22.6094175923108,-39.4753104663248));
#70145=CARTESIAN_POINT('Ctrl Pts',(-20.6079206126006,26.3892496042072,-39.2764235549498));
#70146=CARTESIAN_POINT('Ctrl Pts',(-24.34829326562,27.5602840137214,-39.077536643575));
#70147=CARTESIAN_POINT('Ctrl Pts',(-27.3553341468577,25.0464394858545,-38.8786497322));
#70148=CARTESIAN_POINT('Ctrl Pts',(-26.8658276414789,21.1577260028483,-38.6797628208252));
#70149=CARTESIAN_POINT('Ctrl Pts',(-23.3295887246191,19.467541547054,-38.4808759094503));
#70150=CARTESIAN_POINT('Ctrl Pts',(-19.9961211372559,21.5290223293364,-38.2819889980755));
#70151=CARTESIAN_POINT('Ctrl Pts',(-19.9285989607326,25.4478422955252,-38.0831020867004));
#70152=CARTESIAN_POINT('Ctrl Pts',(-23.1890693503378,27.6229381578333,-37.8842151753257));
#70153=CARTESIAN_POINT('Ctrl Pts',(-26.7814364603257,26.0555812365168,-37.6853282639507));
#70154=CARTESIAN_POINT('Ctrl Pts',(-27.4046194991203,22.1860396523133,-37.4864413525758));
#70155=CARTESIAN_POINT('Ctrl Pts',(-24.485966091278,19.5700940380829,-37.287554441201));
#70156=CARTESIAN_POINT('Ctrl Pts',(-20.7074712576047,20.6115766176912,-37.088667529826));
#70157=CARTESIAN_POINT('Ctrl Pts',(-19.5412513867153,24.353453203639,-36.8897806184512));
#70158=CARTESIAN_POINT('Ctrl Pts',(-22.0589636608176,27.3572564722562,-36.6908937070762));
#70159=CARTESIAN_POINT('Ctrl Pts',(-25.9470439668104,26.862745900202,-36.4920067957014));
#70160=CARTESIAN_POINT('Ctrl Pts',(-27.6326761583333,23.3243347756119,-36.2931198843265));
#70161=CARTESIAN_POINT('Ctrl Pts',(-25.5669071694184,19.9935229141944,-36.0942329729517));
#70162=CARTESIAN_POINT('Ctrl Pts',(-21.6480035525516,19.9310440103175,-35.8953460615767));
#70163=CARTESIAN_POINT('Ctrl Pts',(-19.4771054634003,23.1943108793065,-35.6964591502018));
#70164=CARTESIAN_POINT('Ctrl Pts',(-21.0490841840901,26.7846579479644,-35.4975722388269));
#70165=CARTESIAN_POINT('Ctrl Pts',(-24.9194245521232,27.4028606714261,-35.2986853274521));
#70166=CARTESIAN_POINT('Ctrl Pts',(-27.5316119200257,24.4808431617777,-35.0997984160771));
#70167=CARTESIAN_POINT('Ctrl Pts',(-26.4852675736608,20.7036917641565,-34.9009115047023));
#70168=CARTESIAN_POINT('Ctrl Pts',(-22.741893251967,19.5422883633496,-34.7020245933273));
#70169=CARTESIAN_POINT('Ctrl Pts',(-19.741332570778,22.0638642139288,-34.5031376819525));
#70170=CARTESIAN_POINT('Ctrl Pts',(-20.2408463905141,25.9513049035876,-34.3042507705776));
#70171=CARTESIAN_POINT('Ctrl Pts',(-23.7814238626257,27.6323820391462,-34.1053638592027));
#70172=CARTESIAN_POINT('Ctrl Pts',(-27.1095744817079,25.5623282648628,-33.9064769478278));
#70173=CARTESIAN_POINT('Ctrl Pts',(-27.1670100094627,21.643347487687,-33.7075900364529));
#70174=CARTESIAN_POINT('Ctrl Pts',(-23.9009520656134,19.4766507670683,-33.508703125078));
#70175=CARTESIAN_POINT('Ctrl Pts',(-20.3126309845092,21.0532486836677,-33.3098162137031));
#70176=CARTESIAN_POINT('Ctrl Pts',(-19.699409600229,24.92438142559,-33.1109293023283));
#70177=CARTESIAN_POINT('Ctrl Pts',(-22.6247863723266,27.5328062209393,-32.9120423909533));
#70178=CARTESIAN_POINT('Ctrl Pts',(-26.4005880782925,26.4816018407416,-32.7131554795785));
#70179=CARTESIAN_POINT('Ctrl Pts',(-27.5571730855357,22.7367359829647,-32.5142685682036));
#70180=CARTESIAN_POINT('Ctrl Pts',(-25.0317378346372,19.7394228586415,-32.3153816568287));
#70181=CARTESIAN_POINT('Ctrl Pts',(-21.1449431995737,20.24393909878,-32.1164947454538));
#70182=CARTESIAN_POINT('Ctrl Pts',(-19.4684239041284,23.786677054616,-31.9176078340789));
#70183=CARTESIAN_POINT('Ctrl Pts',(-21.54275903542,27.1121609193807,-31.718720922704));
#70184=CARTESIAN_POINT('Ctrl Pts',(-25.4618104824077,27.1645529758905,-31.5198340113291));
#70185=CARTESIAN_POINT('Ctrl Pts',(-27.6243022460767,23.8957093663268,-31.3209470999543));
#70186=CARTESIAN_POINT('Ctrl Pts',(-26.0430877446809,20.3094202156451,-31.1220601885793));
#70187=CARTESIAN_POINT('Ctrl Pts',(-22.1711690401219,19.701181186145,-30.9231732772045));
#70188=CARTESIAN_POINT('Ctrl Pts',(-19.5665111373198,22.6299123757717,-30.7242863658296));
#70189=CARTESIAN_POINT('Ctrl Pts',(-20.6225738103778,26.4043581367141,-30.5253994544547));
#70190=CARTESIAN_POINT('Ctrl Pts',(-24.3689250021044,27.5561228348926,-30.3265125430798));
#70191=CARTESIAN_POINT('Ctrl Pts',(-27.362985605503,25.0268323662238,-30.1276256317049));
#70192=CARTESIAN_POINT('Ctrl Pts',(-26.8534677805267,21.1406902229469,-29.92873872033));
#70193=CARTESIAN_POINT('Ctrl Pts',(-23.3085752083413,19.4687315442152,-29.7298518089551));
#70194=CARTESIAN_POINT('Ctrl Pts',(-19.9857636054592,21.5473445970642,-29.5309648975802));
#70195=CARTESIAN_POINT('Ctrl Pts',(-19.9384151069646,25.4664602232498,-29.3320779862053));
#70196=CARTESIAN_POINT('Ctrl Pts',(-23.2100389684831,27.6247434485159,-29.1331910748305));
#70197=CARTESIAN_POINT('Ctrl Pts',(-26.7942902492392,26.0389149810833,-28.9343041634555));
#70198=CARTESIAN_POINT('Ctrl Pts',(-27.3975459166122,22.1662167264417,-28.7354172520807));
#70199=CARTESIAN_POINT('Ctrl Pts',(-24.4654651599321,19.5653300299422,-28.5365303407058));
#70200=CARTESIAN_POINT('Ctrl Pts',(-20.6923815951358,20.6262492468413,-28.3376434293309));
#70201=CARTESIAN_POINT('Ctrl Pts',(-19.5454391135397,24.3740795679248,-28.138756517956));
#70202=CARTESIAN_POINT('Ctrl Pts',(-22.0785806110445,27.3648826917262,-27.9398696065811));
#70203=CARTESIAN_POINT('Ctrl Pts',(-25.9640638264242,26.85036412576,-27.7409826952062));
#70204=CARTESIAN_POINT('Ctrl Pts',(-27.6314591193952,23.3033228081687,-27.5420957838313));
#70205=CARTESIAN_POINT('Ctrl Pts',(-25.5485715875246,19.9831889703093,-27.3432088724564));
#70206=CARTESIAN_POINT('Ctrl Pts',(-21.6293982728614,19.9408841082468,-27.1443219610815));
#70207=CARTESIAN_POINT('Ctrl Pts',(-19.4753271604816,23.215282803356,-26.9454350497067));
#70208=CARTESIAN_POINT('Ctrl Pts',(-21.0657669675498,26.7974902780584,-26.7465481383317));
#70209=CARTESIAN_POINT('Ctrl Pts',(-24.9392383584286,27.3957615842105,-26.5476612269569));
#70210=CARTESIAN_POINT('Ctrl Pts',(-27.5363495411159,24.4603361165003,-26.3487743155819));
#70211=CARTESIAN_POINT('Ctrl Pts',(-26.4705755374379,20.6886209967165,-26.1498874042071));
#70212=CARTESIAN_POINT('Ctrl Pts',(-22.7212722940406,19.546502631234,-25.9510004928322));
#70213=CARTESIAN_POINT('Ctrl Pts',(-19.7337316031135,22.0834909622628,-25.7521135814573));
#70214=CARTESIAN_POINT('Ctrl Pts',(-20.2532500579395,25.9683088147261,-25.5532266700824));
#70215=CARTESIAN_POINT('Ctrl Pts',(-23.8024342464345,27.6311379604468,-25.3543397587075));
#70216=CARTESIAN_POINT('Ctrl Pts',(-27.1198848205667,25.5439793991697,-25.1554528473327));
#70217=CARTESIAN_POINT('Ctrl Pts',(-27.1571459761329,21.6247548868448,-24.9565659359577));
#70218=CARTESIAN_POINT('Ctrl Pts',(-23.8799778703928,19.4748994548584,-24.7576790245828));
#70219=CARTESIAN_POINT('Ctrl Pts',(-20.2998201344873,21.0699479675242,-24.558792113208));
#70220=CARTESIAN_POINT('Ctrl Pts',(-19.7065341803949,24.9441860795144,-24.3599052018331));
#70221=CARTESIAN_POINT('Ctrl Pts',(-22.6452994975725,27.537517447133,-24.1610182904582));
#70222=CARTESIAN_POINT('Ctrl Pts',(-26.415639925744,26.4668904217786,-23.9621313790834));
#70223=CARTESIAN_POINT('Ctrl Pts',(-27.5529322835708,22.7161204655495,-23.7632444677084));
#70224=CARTESIAN_POINT('Ctrl Pts',(-25.0121013207012,19.7318471553711,-23.5643575563335));
#70225=CARTESIAN_POINT('Ctrl Pts',(-21.1279552650718,20.256364638646,-23.3654706449586));
#70226=CARTESIAN_POINT('Ctrl Pts',(-19.4696950205286,23.8076858199938,-23.1665837335838));
#70227=CARTESIAN_POINT('Ctrl Pts',(-21.5611211545233,27.1224476361376,-22.9676968222088));
#70228=CARTESIAN_POINT('Ctrl Pts',(-25.4803903736092,27.1546650234968,-22.768809910834));
#70229=CARTESIAN_POINT('Ctrl Pts',(-27.626026564677,23.8747329346722,-22.569922999459));
#70230=CARTESIAN_POINT('Ctrl Pts',(-26.0263719880847,20.2966308669121,-22.3710360880842));
#70231=CARTESIAN_POINT('Ctrl Pts',(-22.1513735713785,19.7083312474613,-22.1721491767093));
#70232=CARTESIAN_POINT('Ctrl Pts',(-19.5618263138254,22.6504315470131,-21.9732622653344));
#70233=CARTESIAN_POINT('Ctrl Pts',(-20.6373045877163,26.4193910392483,-21.7743753539595));
#70234=CARTESIAN_POINT('Ctrl Pts',(-24.3895350448656,27.5518555058708,-21.5754884425846));
#70235=CARTESIAN_POINT('Ctrl Pts',(-27.3705360318328,25.0071861192072,-21.3766015312098));
#70236=CARTESIAN_POINT('Ctrl Pts',(-26.8410203887985,21.1237182932167,-21.1777146198348));
#70237=CARTESIAN_POINT('Ctrl Pts',(-23.2875680961884,19.470029696211,-20.97882770846));
#70238=CARTESIAN_POINT('Ctrl Pts',(-19.9755005278409,21.5657199391672,-20.779940797085));
#70239=CARTESIAN_POINT('Ctrl Pts',(-19.9483269620463,25.4850273740393,-20.5810538857102));
#70240=CARTESIAN_POINT('Ctrl Pts',(-23.2310176018315,27.6264407706511,-20.3821669743353));
#70241=CARTESIAN_POINT('Ctrl Pts',(-26.807058075502,26.0221827794312,-20.1832800629604));
#70242=CARTESIAN_POINT('Ctrl Pts',(-27.3903703859868,22.1464304756638,-19.9843931515855));
#70243=CARTESIAN_POINT('Ctrl Pts',(-24.4449399766786,19.560671616906,-19.7855062402106));
#70244=CARTESIAN_POINT('Ctrl Pts',(-20.6773676624156,20.6409993581589,-19.5866193288357));
#70245=CARTESIAN_POINT('Ctrl Pts',(-19.549732962551,24.3946841018984,-19.3877324174608));
#70246=CARTESIAN_POINT('Ctrl Pts',(-22.0982365586042,27.3724078286106,-19.1888455060859));
#70247=CARTESIAN_POINT('Ctrl Pts',(-25.9810197232746,26.837894902785,-18.9899585947111));
#70248=CARTESIAN_POINT('Ctrl Pts',(-27.6301339339536,23.2823173840323,-18.7910716833361));
#70249=CARTESIAN_POINT('Ctrl Pts',(-25.5301830528546,19.9729495488268,-18.5921847719613));
#70250=CARTESIAN_POINT('Ctrl Pts',(-21.6108438932343,19.9508198496008,-18.3932978605864));
#70251=CARTESIAN_POINT('Ctrl Pts',(-19.4736568376225,23.236263603654,-18.1944109492115));
#70252=CARTESIAN_POINT('Ctrl Pts',(-21.0825155865463,26.8102365607052,-17.9955240378366));
#70253=CARTESIAN_POINT('Ctrl Pts',(-24.9590153584717,27.3885605961603,-17.7966371264617));
#70254=CARTESIAN_POINT('Ctrl Pts',(-27.540981535979,24.4398049552278,-17.5977502150868));
#70255=CARTESIAN_POINT('Ctrl Pts',(-26.4558061165702,20.6736260586761,-17.3988633037119));
#70256=CARTESIAN_POINT('Ctrl Pts',(-22.7006733029792,19.5508229931235,-17.199976392337));
#70257=CARTESIAN_POINT('Ctrl Pts',(-19.7262317681373,22.1031565778123,-17.0010894809621));
#70258=CARTESIAN_POINT('Ctrl Pts',(-20.2657410915107,25.9852486506146,-16.8022025695872));
#70259=CARTESIAN_POINT('Ctrl Pts',(-23.8234379477659,27.6297857437541,-16.6033156582124));
#70260=CARTESIAN_POINT('Ctrl Pts',(-27.1301005689551,25.5255777023874,-16.4044287468375));
#70261=CARTESIAN_POINT('Ctrl Pts',(-27.1471863649619,21.6062133091092,-16.2055418354626));
#70262=CARTESIAN_POINT('Ctrl Pts',(-23.8589949378929,19.473256134042,-16.0066549240877));
#70263=CARTESIAN_POINT('Ctrl Pts',(-20.2870954165664,21.0867129761265,-15.8077680127128));
#70264=CARTESIAN_POINT('Ctrl Pts',(-19.7137606139441,24.9639537960686,-15.6088811013379));
#70265=CARTESIAN_POINT('Ctrl Pts',(-22.665836602861,27.5421230161513,-15.409994189963));
#70266=CARTESIAN_POINT('Ctrl Pts',(-26.4306158442705,26.4521017158213,-15.2111072785881));
#70267=CARTESIAN_POINT('Ctrl Pts',(-27.5485854159584,22.6955270515157,-15.0122203672132));
#70268=CARTESIAN_POINT('Ctrl Pts',(-24.9924260697318,19.7243726347242,-14.8133334558383));
#70269=CARTESIAN_POINT('Ctrl Pts',(-21.1110315182003,20.2688774621258,-14.6144465444634));
#70270=CARTESIAN_POINT('Ctrl Pts',(-19.4710742662327,23.8286877637347,-14.4155596330886));
#70271=CARTESIAN_POINT('Ctrl Pts',(-21.5795359829419,27.132639694513,-14.2166727217137));
#70272=CARTESIAN_POINT('Ctrl Pts',(-25.4989191187454,27.1446815590036,-14.0177858103388));
#70273=CARTESIAN_POINT('Ctrl Pts',(-27.6276428807294,23.8537479047216,-13.8188988989639));
#70274=CARTESIAN_POINT('Ctrl Pts',(-26.0095906176419,20.2839277347915,-13.620011987589));
#70275=CARTESIAN_POINT('Ctrl Pts',(-22.1316151710521,19.7155831145417,-13.4211250762141));
#70276=CARTESIAN_POINT('Ctrl Pts',(-19.5572471782792,22.6709745623044,-13.2222381648392));
#70277=CARTESIAN_POINT('Ctrl Pts',(-20.6521125542706,26.4343479134584,-13.0233512534643));
#70278=CARTESIAN_POINT('Ctrl Pts',(-24.4101228477655,27.5474821397344,-12.8244643420894));
#70279=CARTESIAN_POINT('Ctrl Pts',(-27.3779852257712,24.9875012654034,-12.6255774307145));
#70280=CARTESIAN_POINT('Ctrl Pts',(-26.8284857961336,21.1068106633908,-12.4266905193396));
#70281=CARTESIAN_POINT('Ctrl Pts',(-23.266567944821,19.4714359686424,-12.2278036079647));
#70282=CARTESIAN_POINT('Ctrl Pts',(-19.9653321763585,21.5841478687237,-12.0289166965899));
#70283=CARTESIAN_POINT('Ctrl Pts',(-19.9583342633272,25.5035432558892,-11.830029785215));
#70284=CARTESIAN_POINT('Ctrl Pts',(-23.2520046944779,27.6280300792623,-11.6311428738401));
#70285=CARTESIAN_POINT('Ctrl Pts',(-26.8197396007837,26.0053850749412,-11.4322559624652));
#70286=CARTESIAN_POINT('Ctrl Pts',(-27.3830930973862,22.1266814242883,-11.2333690510903));
#70287=CARTESIAN_POINT('Ctrl Pts',(-24.4243910854073,19.5561189224158,-11.0344821397154));
#70288=CARTESIAN_POINT('Ctrl Pts',(-20.6624298572932,20.6558265607855,-10.8355952283405));
#70289=CARTESIAN_POINT('Ctrl Pts',(-19.5541328199681,24.4152662595675,-10.6367083169656));
#70290=CARTESIAN_POINT('Ctrl Pts',(-22.117930982641,27.3798316835035,-10.4378214055907));
#70291=CARTESIAN_POINT('Ctrl Pts',(-25.9979112080529,26.825338561694,-10.2389344942159));
#70292=CARTESIAN_POINT('Ctrl Pts',(-27.6287006371241,23.2613190598182,-10.040047582841));
#70293=CARTESIAN_POINT('Ctrl Pts',(-25.5117420526801,19.9628049210777,-9.84116067146604));
#70294=CARTESIAN_POINT('Ctrl Pts',(-21.5923409053361,19.9608509710958,-9.64227376009116));
#70295=CARTESIAN_POINT('Ctrl Pts',(-19.4720945390846,23.2572527242379,-9.44338684871627));
#70296=CARTESIAN_POINT('Ctrl Pts',(-21.099329597264,26.8228964581455,-9.24449993734137));
#70297=CARTESIAN_POINT('Ctrl Pts',(-24.9787550281883,27.3812578980914,-9.04561302596649));
#70298=CARTESIAN_POINT('Ctrl Pts',(-27.5455077818732,24.4192502220087,-8.84672611459159));
#70299=CARTESIAN_POINT('Ctrl Pts',(-26.4409597024275,20.6587073473808,-8.64783920321671));
#70300=CARTESIAN_POINT('Ctrl Pts',(-22.6800968246285,19.5552493345345,-8.44895229184182));
#70301=CARTESIAN_POINT('Ctrl Pts',(-19.7188332645852,22.1228605394645,-8.25006538046692));
#70302=CARTESIAN_POINT('Ctrl Pts',(-20.2783191602318,26.0021239623703,-8.05117846909204));
#70303=CARTESIAN_POINT('Ctrl Pts',(-23.8444344100502,27.6283254249002,-7.85229155771715));
#70304=CARTESIAN_POINT('Ctrl Pts',(-27.1402214561694,25.507123662136,-7.65340464634224));
#70305=CARTESIAN_POINT('Ctrl Pts',(-27.1371314398662,21.5877232458067,-7.45451773496737));
#70306=CARTESIAN_POINT('Ctrl Pts',(-23.8380038241329,19.4717208481646,-7.25563082359246));
#70307=CARTESIAN_POINT('Ctrl Pts',(-20.2744571679346,21.1035432652248,-7.05674391221759));
#70308=CARTESIAN_POINT('Ctrl Pts',(-19.7210887093864,24.9836840514344,-6.85785700084268));
#70309=CARTESIAN_POINT('Ctrl Pts',(-22.6863971439858,27.5466228059533,-6.65897008946781));
#70310=CARTESIAN_POINT('Ctrl Pts',(-26.4455154370305,26.4372361147506,-6.4600831780929));
#70311=CARTESIAN_POINT('Ctrl Pts',(-27.5441325978844,22.6749562865615,-6.26119626671804));
#70312=CARTESIAN_POINT('Ctrl Pts',(-24.9727126030969,19.7169994947659,-6.06230935534312));
#70313=CARTESIAN_POINT('Ctrl Pts',(-21.0941724074158,20.2814772376461,-5.86342244396824));
#70314=CARTESIAN_POINT('Ctrl Pts',(-19.4725616046925,23.8496823293152,-5.66453553259335));
#70315=CARTESIAN_POINT('Ctrl Pts',(-21.598003032707,27.1427368244307,-5.46564862121845));
#70316=CARTESIAN_POINT('Ctrl Pts',(-25.5173962268293,27.1346028469598,-5.26676170984357));
#70317=CARTESIAN_POINT('Ctrl Pts',(-27.6291511514034,23.8327548325505,-5.06787479846868));
#70318=CARTESIAN_POINT('Ctrl Pts',(-25.9927440780369,20.2713111558993,-4.86898788709378));
#70319=CARTESIAN_POINT('Ctrl Pts',(-22.111894362714,19.7229365952208,-4.6701009757189));
#70320=CARTESIAN_POINT('Ctrl Pts',(-19.552773852022,22.6915408772831,-4.471214064344));
#70321=CARTESIAN_POINT('Ctrl Pts',(-20.6669973176491,26.4492283630071,-4.27232715296912));
#70322=CARTESIAN_POINT('Ctrl Pts',(-24.4306878652549,27.5430028523719,-4.07344024159422));
#70323=CARTESIAN_POINT('Ctrl Pts',(-27.3853329899243,24.9677783264349,-3.87455333021934));
#70324=CARTESIAN_POINT('Ctrl Pts',(-26.8158643346817,21.0899677814989,-3.67566641884444));
#70325=CARTESIAN_POINT('Ctrl Pts',(-23.2455753107149,19.4729503242449,-3.47677950746956));
#70326=CARTESIAN_POINT('Ctrl Pts',(-19.9552588204597,21.602627897418,-3.27789259609466));
#70327=CARTESIAN_POINT('Ctrl Pts',(-19.9684367456271,25.5220073781535,-3.07900568471977));
#70328=CARTESIAN_POINT('Ctrl Pts',(-23.272999690292,27.6295113322349,-2.88011877334488));
#70329=CARTESIAN_POINT('Ctrl Pts',(-26.8323344890412,25.98852231273,-2.68123186196999));
#70330=CARTESIAN_POINT('Ctrl Pts',(-27.3757142436486,22.106970095639,-2.4823449505951));
#70331=CARTESIAN_POINT('Ctrl Pts',(-24.4038190306359,19.5516720671119,-2.28345803922021));
#70332=CARTESIAN_POINT('Ctrl Pts',(-20.6475685756005,20.6707304618203,-2.08457112784532));
#70333=CARTESIAN_POINT('Ctrl Pts',(-19.5586385692006,24.4358254955324,-1.88568421647042));
#70334=CARTESIAN_POINT('Ctrl Pts',(-22.1376633612786,27.3871540596825,-1.68679730509554));
#70335=CARTESIAN_POINT('Ctrl Pts',(-26.0147378331575,26.8126954352138,-1.48791039372065));
#70336=CARTESIAN_POINT('Ctrl Pts',(-27.627159266887,23.2403283919536,-1.28902348234576));
#70337=CARTESIAN_POINT('Ctrl Pts',(-25.4932490756625,19.9527553558813,-1.09013657097086));
#70338=CARTESIAN_POINT('Ctrl Pts',(-21.5738897994712,19.9709772069203,-0.891249659595981));
#70339=CARTESIAN_POINT('Ctrl Pts',(-19.4706403062664,23.278249608924,-0.692362748221079));
#70340=CARTESIAN_POINT('Ctrl Pts',(-21.1162085541538,26.8354696349089,-0.493475836846195));
#70341=CARTESIAN_POINT('Ctrl Pts',(-24.9984568445039,27.3738536835161,-0.294588925471298));
#70342=CARTESIAN_POINT('Ctrl Pts',(-27.549928158859,24.3986724615157,-0.0957020140964179));
#70343=CARTESIAN_POINT('Ctrl Pts',(-26.4260366884199,20.6438652581567,0.103184897278475));
#70344=CARTESIAN_POINT('Ctrl Pts',(-22.6595434042374,19.5597815381747,0.30207180865337));
#70345=CARTESIAN_POINT('Ctrl Pts',(-19.7115362885075,22.1426023250911,0.500958720028255));
#70346=CARTESIAN_POINT('Ctrl Pts',(-20.2909839308012,26.0189343028199,0.699845631403148));
#70347=CARTESIAN_POINT('Ctrl Pts',(-23.865423076909,27.6267570425813,0.898732542778043));
#70348=CARTESIAN_POINT('Ctrl Pts',(-27.1502472140198,25.4886177674228,1.09761945415293));
#70349=CARTESIAN_POINT('Ctrl Pts',(-27.1269814672878,21.5692851868996,1.29650636552782));
#70350=CARTESIAN_POINT('Ctrl Pts',(-23.8170050853494,19.4702936379094,1.49539327690272));
#70351=CARTESIAN_POINT('Ctrl Pts',(-20.2619057234888,21.1204383888387,1.6942801882776));
#70352=CARTESIAN_POINT('Ctrl Pts',(-19.7285182725368,25.0033763227863,1.89316709965249));
#70353=CARTESIAN_POINT('Ctrl Pts',(-22.7069805761205,27.5510166973002,2.09205401102739));
#70354=CARTESIAN_POINT('Ctrl Pts',(-26.4603383092049,26.4222940124852,2.29094092240227));
#70355=CARTESIAN_POINT('Ctrl Pts',(-27.5395739473425,22.6544087157843,2.48982783377716));
#70356=CARTESIAN_POINT('Ctrl Pts',(-24.9529614431771,19.7097279308745,2.68871474515205));
#70357=CARTESIAN_POINT('Ctrl Pts',(-21.077378379462,20.2941636313296,2.88760165652695));
#70358=CARTESIAN_POINT('Ctrl Pts',(-19.4741569964957,23.8706689604074,3.08648856790183));
#70359=CARTESIAN_POINT('Ctrl Pts',(-21.6165218144668,27.1527387583308,3.28537547927672));
#70360=CARTESIAN_POINT('Ctrl Pts',(-25.5358212082423,27.1244291544376,3.48426239065162));
#70361=CARTESIAN_POINT('Ctrl Pts',(-27.6305513367319,23.8117542744471,3.68314930202651));
#70362=CARTESIAN_POINT('Ctrl Pts',(-25.9758328156801,20.2587814645581,3.88203621340138));
#70363=CARTESIAN_POINT('Ctrl Pts',(-22.0922116689392,19.7303914946417,4.08092312477631));
#70364=CARTESIAN_POINT('Ctrl Pts',(-19.5484064535911,22.7121299469694,4.27981003615117));
#70365=CARTESIAN_POINT('Ctrl Pts',(-20.6819584834256,26.4640319935825,4.47869694752607));
#70366=CARTESIAN_POINT('Ctrl Pts',(-24.451229552388,27.5384177624785,4.67758385890096));
#70367=CARTESIAN_POINT('Ctrl Pts',(-27.3925791295866,24.9480178249331,4.87647077027585));
#70368=CARTESIAN_POINT('Ctrl Pts',(-26.8031563388947,21.0731900938547,5.07535768165073));
#70369=CARTESIAN_POINT('Ctrl Pts',(-23.2245907501465,19.47457272289,5.27424459302565));
#70370=CARTESIAN_POINT('Ctrl Pts',(-19.9452807270751,21.6211595355544,5.47313150440051));
#70371=CARTESIAN_POINT('Ctrl Pts',(-19.9786341412437,25.5404192515574,5.67201841577542));
#70372=CARTESIAN_POINT('Ctrl Pts',(-23.294002032935,27.6308844903178,5.87090532715031));
#70373=CARTESIAN_POINT('Ctrl Pts',(-26.8448424065264,25.971594939638,6.06979223852519));
#70374=CARTESIAN_POINT('Ctrl Pts',(-27.3682340203038,22.0872970120394,6.26867914990007));
#70375=CARTESIAN_POINT('Ctrl Pts',(-24.3832243574966,19.54733116883,6.46756606127497));
#70376=CARTESIAN_POINT('Ctrl Pts',(-20.6327842111413,20.6857106663298,6.66645297264987));
#70377=CARTESIAN_POINT('Ctrl Pts',(-19.5632500908522,24.4563612650009,6.86533988402474));
#70378=CARTESIAN_POINT('Ctrl Pts',(-22.1574331716357,27.3943747631147,7.06422679539965));
#70379=CARTESIAN_POINT('Ctrl Pts',(-26.0314991527055,26.7999658583701,7.26311370677453));
#70380=CARTESIAN_POINT('Ctrl Pts',(-27.6255098640867,23.2193459366633,7.46200061814942));
#70381=CARTESIAN_POINT('Ctrl Pts',(-25.4747046118414,19.9428011195373,7.66088752952431));
#70382=CARTESIAN_POINT('Ctrl Pts',(-21.5554910645695,19.9811982887427,7.85977444089922));
#70383=CARTESIAN_POINT('Ctrl Pts',(-19.4692941777034,23.2992537013228,8.05866135227408));
#70384=CARTESIAN_POINT('Ctrl Pts',(-21.133152009946,26.8479557578229,8.257548263649));
#70385=CARTESIAN_POINT('Ctrl Pts',(-25.0181202853465,27.366348148636,8.45643517502387));
#70386=CARTESIAN_POINT('Ctrl Pts',(-27.5542425498025,24.3780722190318,8.65532208639878));
#70387=CARTESIAN_POINT('Ctrl Pts',(-26.4110374699872,20.6291001842993,8.85420899777365));
#70388=CARTESIAN_POINT('Ctrl Pts',(-22.6390135864442,19.5644194839469,9.05309590914856));
#70389=CARTESIAN_POINT('Ctrl Pts',(-19.7043410332642,22.1623814115612,9.25198282052343));
#70390=CARTESIAN_POINT('Ctrl Pts',(-20.3037350676194,26.0356792265119,9.45086973189833));
#70391=CARTESIAN_POINT('Ctrl Pts',(-23.8864033921708,27.6250806383578,9.64975664327322));
#70392=CARTESIAN_POINT('Ctrl Pts',(-27.1601775768371,25.4700605086295,9.84864355464811));
#70393=CARTESIAN_POINT('Ctrl Pts',(-27.1167367161873,21.5508996209716,10.047530466023));
#70394=CARTESIAN_POINT('Ctrl Pts',(-23.7959992779809,19.4689745410956,10.2464173773979));
#70395=CARTESIAN_POINT('Ctrl Pts',(-20.2494414158251,21.1373978992702,10.4453042887728));
#70396=CARTESIAN_POINT('Ctrl Pts',(-19.7360491065219,25.0230300883058,10.6441912001477));
#70397=CARTESIAN_POINT('Ctrl Pts',(-22.7275863538313,27.5553045737599,10.8430781115225));
#70398=CARTESIAN_POINT('Ctrl Pts',(-26.4750840680073,26.4072758049705,11.0419650228975));
#70399=CARTESIAN_POINT('Ctrl Pts',(-27.534909585131,22.6338848836673,11.2408519342723));
#70400=CARTESIAN_POINT('Ctrl Pts',(-24.9331731133515,19.7025581357365,11.4397388456472));
#70401=CARTESIAN_POINT('Ctrl Pts',(-21.0606498793582,20.3069363070043,11.6386257570221));
#70402=CARTESIAN_POINT('Ctrl Pts',(-19.4758603993663,23.8916471008938,11.837512668397));
#70403=CARTESIAN_POINT('Ctrl Pts',(-21.6350918374984,27.1626452311751,12.0363995797719));
#70404=CARTESIAN_POINT('Ctrl Pts',(-25.5541935747473,27.1141607510261,12.2352864911468));
#70405=CARTESIAN_POINT('Ctrl Pts',(-27.6318433996117,23.790746786898,12.4341734025216));
#70406=CARTESIAN_POINT('Ctrl Pts',(-25.9588572786975,20.2463389927879,12.6330603138966));
#70407=CARTESIAN_POINT('Ctrl Pts',(-22.0725676112927,19.7379476152593,12.8319472252714));
#70408=CARTESIAN_POINT('Ctrl Pts',(-19.5441450987166,22.7327412257809,13.0308341366463));
#70409=CARTESIAN_POINT('Ctrl Pts',(-20.6969956551495,26.4787584129081,13.2297210480212));
#70410=CARTESIAN_POINT('Ctrl Pts',(-24.4717473648378,27.5337269915527,13.4286079593961));
#70411=CARTESIAN_POINT('Ctrl Pts',(-27.3997234527448,24.9282202845247,13.627494870771));
#70412=CARTESIAN_POINT('Ctrl Pts',(-26.7903621455173,21.0564780450445,13.8263817821459));
#70413=CARTESIAN_POINT('Ctrl Pts',(-23.203614819179,19.4763031215864,14.0252686935208));
#70414=CARTESIAN_POINT('Ctrl Pts',(-19.9353981606106,21.639742292069,14.2241556048957));
#70415=CARTESIAN_POINT('Ctrl Pts',(-19.9889261799598,25.5587783882113,14.4230425162706));
#70416=CARTESIAN_POINT('Ctrl Pts',(-23.3150111658725,27.632149517124,14.6219294276455));
#70417=CARTESIAN_POINT('Ctrl Pts',(-26.8572630217964,25.9546034042184,14.8208163390203));
#70418=CARTESIAN_POINT('Ctrl Pts',(-27.3606526255678,22.0676626947997,15.0197032503953));
#70419=CARTESIAN_POINT('Ctrl Pts',(-24.3626076117206,19.5430963425982,15.2185901617701));
#70420=CARTESIAN_POINT('Ctrl Pts',(-20.6180771556817,20.7007667773587,15.417477073145));
#70421=CARTESIAN_POINT('Ctrl Pts',(-19.5679672627237,24.4768730238026,15.6163639845199));
#70422=CARTESIAN_POINT('Ctrl Pts',(-22.1772398898387,27.4014936024608,15.8152508958948));
#70423=CARTESIAN_POINT('Ctrl Pts',(-26.048194722544,26.7871501684795,16.0141378072697));
#70424=CARTESIAN_POINT('Ctrl Pts',(-27.6237524724303,23.1983722499541,16.2130247186446));
#70425=CARTESIAN_POINT('Ctrl Pts',(-25.4561091526197,19.9329424758199,16.4119116300195));
#70426=CARTESIAN_POINT('Ctrl Pts',(-21.5371451881725,19.9915139457182,16.6107985413944));
#70427=CARTESIAN_POINT('Ctrl Pts',(-19.468056189066,23.3202644448542,16.8096854527693));
#70428=CARTESIAN_POINT('Ctrl Pts',(-21.1501595156618,26.8603544960221,17.0085723641442));
#70429=CARTESIAN_POINT('Ctrl Pts',(-25.0377448296613,27.3587414923376,17.207459275519));
#70430=CARTESIAN_POINT('Ctrl Pts',(-27.558450840378,24.3574500404358,17.4063461868939));
#70431=CARTESIAN_POINT('Ctrl Pts',(-26.3959624445887,20.6144125170631,17.6052330982688));
#70432=CARTESIAN_POINT('Ctrl Pts',(-22.6185079152614,19.5691630489516,17.8041200096437));
#70433=CARTESIAN_POINT('Ctrl Pts',(-19.69724768952,22.1821972747556,18.0030069210186));
#70434=CARTESIAN_POINT('Ctrl Pts',(-20.3165722327983,26.0523582897283,18.2018938323935));
#70435=CARTESIAN_POINT('Ctrl Pts',(-23.9073747998855,27.6232962566519,18.4007807437684));
#70436=CARTESIAN_POINT('Ctrl Pts',(-27.17001228148,25.4514523774982,18.5996676551433));
#70437=CARTESIAN_POINT('Ctrl Pts',(-27.1063974580369,21.5325670352153,18.7985545665182));
#70438=CARTESIAN_POINT('Ctrl Pts',(-23.7749869586531,19.4677635926774,18.9974414778931));
#70439=CARTESIAN_POINT('Ctrl Pts',(-20.2370645752311,21.1544213471147,19.1963283892679));
#70440=CARTESIAN_POINT('Ctrl Pts',(-19.7436810117847,25.0426448271945,19.3952153006428));
#70441=CARTESIAN_POINT('Ctrl Pts',(-22.7482139310932,27.5594863217094,19.5941022120177));
#70442=CARTESIAN_POINT('Ctrl Pts',(-26.4897523226947,26.3921818901693,19.7929891233926));
#70443=CARTESIAN_POINT('Ctrl Pts',(-27.5301396348492,22.6133853340644,19.9918760347675));
#70444=CARTESIAN_POINT('Ctrl Pts',(-24.9133481379843,19.6954902993422,20.1907629461424));
#70445=CARTESIAN_POINT('Ctrl Pts',(-21.0439873503875,20.319794926211,20.3896498575173));
#70446=CARTESIAN_POINT('Ctrl Pts',(-19.4776717681664,23.9126161948818,20.5885367688922));
#70447=CARTESIAN_POINT('Ctrl Pts',(-21.6537126097211,27.1724559804553,20.787423680267));
#70448=CARTESIAN_POINT('Ctrl Pts',(-25.5725128395008,27.1037979088245,20.986310591642));
#70449=CARTESIAN_POINT('Ctrl Pts',(-27.6330273058053,23.7697329265736,21.1851975030168));
#70450=CARTESIAN_POINT('Ctrl Pts',(-25.9418179169176,20.2339840702973,21.3840844143918));
#70451=CARTESIAN_POINT('Ctrl Pts',(-22.0529627103157,19.7456047568468,21.5829713257666));
#70452=CARTESIAN_POINT('Ctrl Pts',(-19.5399899003186,22.7533741675459,21.7818582371415));
#70453=CARTESIAN_POINT('Ctrl Pts',(-20.7121084343556,26.4934072307538,21.9807451485164));
#70454=CARTESIAN_POINT('Ctrl Pts',(-24.4922407589099,27.5289306638937,22.1796320598913));
#70455=CARTESIAN_POINT('Ctrl Pts',(-27.4067657700838,24.908386229818,22.3785189712661));
#70456=CARTESIAN_POINT('Ctrl Pts',(-26.777482093579,21.0398320779155,22.5774058826411));
#70457=CARTESIAN_POINT('Ctrl Pts',(-23.1826480736459,19.4781414744804,22.776292794016));
#70458=CARTESIAN_POINT('Ctrl Pts',(-19.9256113829413,21.658375674545,22.9751797053909));
#70459=CARTESIAN_POINT('Ctrl Pts',(-19.9993125890499,25.5770843016201,23.1740666167658));
#70460=CARTESIAN_POINT('Ctrl Pts',(-23.3360265323915,27.6333063791363,23.3729535281406));
#70461=CARTESIAN_POINT('Ctrl Pts',(-26.8695960057205,25.9375481567157,23.5718404395156));
#70462=CARTESIAN_POINT('Ctrl Pts',(-27.3529702603396,22.0480676642185,23.7707273508904));
#70463=CARTESIAN_POINT('Ctrl Pts',(-24.3419693396195,19.538967700605,23.9696142622654));
#70464=CARTESIAN_POINT('Ctrl Pts',(-20.6034477989471,20.7158983959945,24.1685011736402));
#70465=CARTESIAN_POINT('Ctrl Pts',(-19.5727899598007,24.4973602283013,24.3673880850151));
#70466=CARTESIAN_POINT('Ctrl Pts',(-22.1970829910656,27.4085103892746,24.56627499639));
#70467=CARTESIAN_POINT('Ctrl Pts',(-26.0648241002076,26.7742487047758,24.7651619077649));
#70468=CARTESIAN_POINT('Ctrl Pts',(-27.6218871385914,23.1774078882897,24.9640488191398));
#70469=CARTESIAN_POINT('Ctrl Pts',(-25.4374631905537,19.9231796846686,25.1629357305147));
#70470=CARTESIAN_POINT('Ctrl Pts',(-21.5188526567968,20.0019239069524,25.3618226418895));
#70471=CARTESIAN_POINT('Ctrl Pts',(-19.4669263724509,23.3412812781227,25.5607095532645));
#70472=CARTESIAN_POINT('Ctrl Pts',(-21.1672306219631,26.8726655297157,25.7595964646393));
#70473=CARTESIAN_POINT('Ctrl Pts',(-25.057329954898,27.3510338996482,25.9584833760142));
#70474=CARTESIAN_POINT('Ctrl Pts',(-27.5625529238418,24.3368065034171,26.1573702873891));
#70475=CARTESIAN_POINT('Ctrl Pts',(-26.3808120026847,20.5998025866847,26.356257198764));
#70476=CARTESIAN_POINT('Ctrl Pts',(-22.5980269510697,19.5740122188322,26.5551441101389));
#70477=CARTESIAN_POINT('Ctrl Pts',(-19.6902564131246,22.2020491793454,26.7540310215138));
#70478=CARTESIAN_POINT('Ctrl Pts',(-20.3294951468089,26.0689714474631,26.9529179328886));
#70479=CARTESIAN_POINT('Ctrl Pts',(-23.9283366298413,27.6214031951935,27.1518048442636));
#70480=CARTESIAN_POINT('Ctrl Pts',(-27.179751283537,25.4327952824294,27.3506917556384));
#70481=CARTESIAN_POINT('Ctrl Pts',(-27.0959635585929,21.5142852430269,27.5495786670134));
#70482=CARTESIAN_POINT('Ctrl Pts',(-23.7539694549667,19.4666658707645,27.7484655783882));
#70483=CARTESIAN_POINT('Ctrl Pts',(-20.2247740742439,21.1714987533596,27.9473524897632));
#70484=CARTESIAN_POINT('Ctrl Pts',(-19.7514165342425,25.0622380103314,28.146239401138));
#70485=CARTESIAN_POINT('Ctrl Pts',(-22.7688575722315,27.5635278603232,28.3451263125129));
#70486=CARTESIAN_POINT('Ctrl Pts',(-26.5043524826052,26.377076810523,28.5440132238879));
#70487=CARTESIAN_POINT('Ctrl Pts',(-27.5252457221917,22.5927894947073,28.7429001352627));
#70488=CARTESIAN_POINT('Ctrl Pts',(-24.8935219757889,19.6887533114419,28.9417870466376));
#70489=CARTESIAN_POINT('Ctrl Pts',(-21.0273252703961,20.3323072149201,29.1406739580125));
#70490=CARTESIAN_POINT('Ctrl Pts',(-19.4797156270952,23.9343920538674,29.3395608693874));
#70491=CARTESIAN_POINT('Ctrl Pts',(-21.6721482617318,27.1806228264275,29.5384477807623));
#70492=CARTESIAN_POINT('Ctrl Pts',(-25.5912242703431,27.0963164159434,29.7373346921371));
#70493=CARTESIAN_POINT('Ctrl Pts',(-27.63368882695,23.7419436154583,29.9362644892681));
#70494=CARTESIAN_POINT('Ctrl Pts',(-26.4947738687757,21.4036029661271,30.068898649274));
#70495=CARTESIAN_POINT('Ctrl Pts',(-25.5559209586874,20.7348455034229,30.1352371721549));
#70496=CARTESIAN_POINT('Ctrl Pts',(-25.1937408823974,26.8611697506233,-75.136612489095));
#70497=CARTESIAN_POINT('Ctrl Pts',(-26.2970650380044,26.3134966205244,-75.07031685197));
#70498=CARTESIAN_POINT('Ctrl Pts',(-27.8938315288374,24.0378889387849,-74.9377255777202));
#70499=CARTESIAN_POINT('Ctrl Pts',(-26.3051630684163,20.151456014636,-74.7388386663452));
#70500=CARTESIAN_POINT('Ctrl Pts',(-22.1814766999306,19.3993779713237,-74.5399517549704));
#70501=CARTESIAN_POINT('Ctrl Pts',(-19.3173747867214,22.4559707153929,-74.3410648435954));
#70502=CARTESIAN_POINT('Ctrl Pts',(-20.3419839806973,26.5210641768467,-74.1421779322206));
#70503=CARTESIAN_POINT('Ctrl Pts',(-24.3152194831348,27.8546762011371,-73.9432910208456));
#70504=CARTESIAN_POINT('Ctrl Pts',(-27.5852507580641,25.2337121388997,-73.7444041094708));
#70505=CARTESIAN_POINT('Ctrl Pts',(-27.1476008207659,21.065354934915,-73.5455171980958));
#70506=CARTESIAN_POINT('Ctrl Pts',(-23.4042186429317,19.1806391005653,-73.346630286721));
#70507=CARTESIAN_POINT('Ctrl Pts',(-19.7950685065841,21.3111051035031,-73.1477433753461));
#70508=CARTESIAN_POINT('Ctrl Pts',(-19.6365932997354,25.4992225805698,-72.9488564639712));
#70509=CARTESIAN_POINT('Ctrl Pts',(-23.0744501205458,27.8963674907323,-72.7499695525964));
#70510=CARTESIAN_POINT('Ctrl Pts',(-26.9495231811252,26.2998194285406,-72.5510826412214));
#70511=CARTESIAN_POINT('Ctrl Pts',(-27.7009578155723,22.1766428820113,-72.3521957298465));
#70512=CARTESIAN_POINT('Ctrl Pts',(-24.6382445793945,19.3157022412448,-72.1533088184717));
#70513=CARTESIAN_POINT('Ctrl Pts',(-20.5757597645979,20.3459515854474,-71.9544219070967));
#70514=CARTESIAN_POINT('Ctrl Pts',(-19.2465811483552,24.32068324995,-71.7555349957219));
#70515=CARTESIAN_POINT('Ctrl Pts',(-21.8721118853346,27.5874536484677,-71.5566480843469));
#70516=CARTESIAN_POINT('Ctrl Pts',(-26.039711464712,27.1443789201376,-71.3577611729721));
#70517=CARTESIAN_POINT('Ctrl Pts',(-27.9197094241392,23.3986065599842,-71.1588742615972));
#70518=CARTESIAN_POINT('Ctrl Pts',(-25.7845469321506,19.7921841029197,-70.9599873502223));
#70519=CARTESIAN_POINT('Ctrl Pts',(-21.5962573421921,19.6391078406365,-70.7611004388474));
#70520=CARTESIAN_POINT('Ctrl Pts',(-19.2035236497863,23.0800419706175,-70.5622135274725));
#70521=CARTESIAN_POINT('Ctrl Pts',(-20.8050652633841,26.953059722229,-70.3633266160976));
#70522=CARTESIAN_POINT('Ctrl Pts',(-24.9292012202206,27.6991861850648,-70.1644397047228));
#70523=CARTESIAN_POINT('Ctrl Pts',(-27.7862002493743,24.6327943873279,-69.9655527933478));
#70524=CARTESIAN_POINT('Ctrl Pts',(-26.7507224743231,20.5716384111603,-69.766665881973));
#70525=CARTESIAN_POINT('Ctrl Pts',(-22.7742841775203,19.2475762656173,-69.5677789705981));
#70526=CARTESIAN_POINT('Ctrl Pts',(-19.5108950067131,21.8773088025077,-69.3688920592232));
#70527=CARTESIAN_POINT('Ctrl Pts',(-19.9593329204414,26.0443347839142,-69.1700051478483));
#70528=CARTESIAN_POINT('Ctrl Pts',(-23.7075214970733,27.9195106390288,-68.9711182364735));
#70529=CARTESIAN_POINT('Ctrl Pts',(-27.3111932287642,25.7797087453964,-68.7722313250984));
#70530=CARTESIAN_POINT('Ctrl Pts',(-27.4588793350163,21.5912256181414,-68.5733444137237));
#70531=CARTESIAN_POINT('Ctrl Pts',(-24.0148688059276,19.2029221263209,-68.3744575023486));
#70532=CARTESIAN_POINT('Ctrl Pts',(-20.1439153137772,20.8094466842194,-68.1755705909739));
#70533=CARTESIAN_POINT('Ctrl Pts',(-19.4030969151261,24.9345394339248,-67.9766836795989));
#70534=CARTESIAN_POINT('Ctrl Pts',(-22.4731629072885,27.7875898886589,-67.7777967682241));
#70535=CARTESIAN_POINT('Ctrl Pts',(-26.5329829421399,26.7468865793022,-67.5789098568492));
#70536=CARTESIAN_POINT('Ctrl Pts',(-27.851926623626,22.768747610067,-67.3800229454743));
#70537=CARTESIAN_POINT('Ctrl Pts',(-25.2179965364443,19.5087454031162,-67.1811360340994));
#70538=CARTESIAN_POINT('Ctrl Pts',(-21.0515511102707,19.9625455840323,-66.9822491227245));
#70539=CARTESIAN_POINT('Ctrl Pts',(-19.1812004354411,23.7131442624633,-66.7833622113496));
#70540=CARTESIAN_POINT('Ctrl Pts',(-21.3256382025381,27.3140592512587,-66.5844752999747));
#70541=CARTESIAN_POINT('Ctrl Pts',(-25.5143079219386,27.4563549829591,-66.3855883885999));
#70542=CARTESIAN_POINT('Ctrl Pts',(-27.8981772621405,24.0092737448201,-66.1867014772249));
#70543=CARTESIAN_POINT('Ctrl Pts',(-26.286672418287,20.1403909303993,-65.9878145658501));
#70544=CARTESIAN_POINT('Ctrl Pts',(-22.1606297088009,19.4048818189811,-65.7889276544751));
#70545=CARTESIAN_POINT('Ctrl Pts',(-19.3115325529678,22.4786169230698,-65.5900407431003));
#70546=CARTESIAN_POINT('Ctrl Pts',(-20.3574596733955,26.5370942917681,-65.3911538317254));
#70547=CARTESIAN_POINT('Ctrl Pts',(-24.3372927264065,27.8509173253781,-65.1922669203505));
#70548=CARTESIAN_POINT('Ctrl Pts',(-27.5939025704812,25.2127940498356,-64.9933800089756));
#70549=CARTESIAN_POINT('Ctrl Pts',(-27.1347408738959,21.0469360793963,-64.7944930976006));
#70550=CARTESIAN_POINT('Ctrl Pts',(-23.3817383053209,19.1814136823847,-64.5956061862259));
#70551=CARTESIAN_POINT('Ctrl Pts',(-19.7835860231326,21.3304837714386,-64.3967192748508));
#70552=CARTESIAN_POINT('Ctrl Pts',(-19.6466809016576,25.5193331458131,-64.1978323634761));
#70553=CARTESIAN_POINT('Ctrl Pts',(-23.0968271398913,27.8987643863169,-63.998945452101));
#70554=CARTESIAN_POINT('Ctrl Pts',(-26.9636328690584,26.2822819254272,-63.8000585407264));
#70555=CARTESIAN_POINT('Ctrl Pts',(-27.6938314751149,22.1552960895905,-63.6011716293512));
#70556=CARTESIAN_POINT('Ctrl Pts',(-24.6164323497271,19.3101569512449,-63.4022847179766));
#70557=CARTESIAN_POINT('Ctrl Pts',(-20.5593043687083,20.3613061505115,-63.2033978066015));
#70558=CARTESIAN_POINT('Ctrl Pts',(-19.2506041588886,24.3428266960193,-63.0045108952267));
#70559=CARTESIAN_POINT('Ctrl Pts',(-21.8929162536123,27.5960387837198,-62.8056239838518));
#70560=CARTESIAN_POINT('Ctrl Pts',(-26.0581798689496,27.131516331915,-62.6067370724768));
#70561=CARTESIAN_POINT('Ctrl Pts',(-27.9188708985218,23.3761160888048,-62.4078501611021));
#70562=CARTESIAN_POINT('Ctrl Pts',(-25.7651720467354,19.7807324723742,-62.208963249727));
#70563=CARTESIAN_POINT('Ctrl Pts',(-21.5761499548322,19.6492181878627,-62.0100763383523));
#70564=CARTESIAN_POINT('Ctrl Pts',(-19.2011607547684,23.1024237121637,-61.8111894269773));
#70565=CARTESIAN_POINT('Ctrl Pts',(-20.8226181555251,26.9671459519908,-61.6123025156025));
#70566=CARTESIAN_POINT('Ctrl Pts',(-24.9505402827237,27.6920328433528,-61.4134156042276));
#70567=CARTESIAN_POINT('Ctrl Pts',(-27.7917166915486,24.6109747933609,-61.2145286928527));
#70568=CARTESIAN_POINT('Ctrl Pts',(-26.7353471543245,20.5552029193142,-61.0156417814778));
#70569=CARTESIAN_POINT('Ctrl Pts',(-22.7521457103933,19.251627700714,-60.8167548701028));
#70570=CARTESIAN_POINT('Ctrl Pts',(-19.5023367669384,21.8981242385019,-60.6178679587281));
#70571=CARTESIAN_POINT('Ctrl Pts',(-19.9722192046344,26.062786600354,-60.418981047353));
#70572=CARTESIAN_POINT('Ctrl Pts',(-23.7300109027001,27.9186431808668,-60.2200941359784));
#70573=CARTESIAN_POINT('Ctrl Pts',(-27.3226198988076,25.7603191332387,-60.0212072246032));
#70574=CARTESIAN_POINT('Ctrl Pts',(-27.4487431285459,21.571131261538,-59.8223203132285));
#70575=CARTESIAN_POINT('Ctrl Pts',(-23.9924840372717,19.2005880352991,-59.6234334018534));
#70576=CARTESIAN_POINT('Ctrl Pts',(-20.1298516874202,20.8270176905143,-59.4245464904788));
#70577=CARTESIAN_POINT('Ctrl Pts',(-19.4102777112886,24.9558692725355,-59.2256595791036));
#70578=CARTESIAN_POINT('Ctrl Pts',(-22.4949895831295,27.7930782463697,-59.026772667729));
#70579=CARTESIAN_POINT('Ctrl Pts',(-26.549398633158,26.7314901207151,-58.8278857563539));
#70580=CARTESIAN_POINT('Ctrl Pts',(-27.8478467015968,22.7466143752181,-58.6289988449792));
#70581=CARTESIAN_POINT('Ctrl Pts',(-25.1971701037923,19.5002139582432,-58.4301119336041));
#70582=CARTESIAN_POINT('Ctrl Pts',(-21.0331158928126,19.975455603626,-58.2312250222293));
#70583=CARTESIAN_POINT('Ctrl Pts',(-19.1820968349725,23.7356325331063,-58.0323381108544));
#70584=CARTESIAN_POINT('Ctrl Pts',(-21.3450425038916,27.3254609589209,-57.8334511994795));
#70585=CARTESIAN_POINT('Ctrl Pts',(-25.5343892173839,27.4461929250044,-57.6345642881046));
#70586=CARTESIAN_POINT('Ctrl Pts',(-27.9004825437762,23.9868859909083,-57.4356773767298));
#70587=CARTESIAN_POINT('Ctrl Pts',(-26.2690833277458,20.126349928207,-57.2367904653548));
#70588=CARTESIAN_POINT('Ctrl Pts',(-22.1393091289809,19.4120900590421,-57.03790355398));
#70589=CARTESIAN_POINT('Ctrl Pts',(-19.3060722890367,22.5004506439263,-56.8390166426051));
#70590=CARTESIAN_POINT('Ctrl Pts',(-20.3728772449516,26.5534901551472,-56.6401297312301));
#70591=CARTESIAN_POINT('Ctrl Pts',(-24.3594206923845,27.8468089229745,-56.4412428198554));
#70592=CARTESIAN_POINT('Ctrl Pts',(-27.6024072062892,25.1919566551229,-56.2423559084803));
#70593=CARTESIAN_POINT('Ctrl Pts',(-27.1218071403008,21.0285174913962,-56.0434689971056));
#70594=CARTESIAN_POINT('Ctrl Pts',(-23.3592512068966,19.1823390218303,-55.8445820857305));
#70595=CARTESIAN_POINT('Ctrl Pts',(-19.7722092967397,21.3499027298354,-55.6456951743558));
#70596=CARTESIAN_POINT('Ctrl Pts',(-19.6568687942637,25.5394013468506,-55.4468082629808));
#70597=CARTESIAN_POINT('Ctrl Pts',(-23.1192178419824,27.9010408547444,-55.247921351606));
#70598=CARTESIAN_POINT('Ctrl Pts',(-26.9776512238312,26.2646747797727,-55.0490344402311));
#70599=CARTESIAN_POINT('Ctrl Pts',(-27.6865958030936,22.1339848038706,-54.8501475288562));
#70600=CARTESIAN_POINT('Ctrl Pts',(-24.5945916200155,19.3047247901372,-54.6512606174813));
#70601=CARTESIAN_POINT('Ctrl Pts',(-20.542928360123,20.3767448095026,-54.4523737061064));
#70602=CARTESIAN_POINT('Ctrl Pts',(-19.2547410348627,24.3649493564789,-54.2534867947315));
#70603=CARTESIAN_POINT('Ctrl Pts',(-21.9137645758749,27.6045165963777,-54.0545998833566));
#70604=CARTESIAN_POINT('Ctrl Pts',(-26.0765817969876,27.1185589057388,-53.8557129719818));
#70605=CARTESIAN_POINT('Ctrl Pts',(-27.9179166206944,23.3536301998417,-53.6568260606067));
#70606=CARTESIAN_POINT('Ctrl Pts',(-25.7457384634566,19.7693807460924,-53.457939149232));
#70607=CARTESIAN_POINT('Ctrl Pts',(-21.556094881439,19.6594318982475,-53.259052237857));
#70608=CARTESIAN_POINT('Ctrl Pts',(-19.1989131033193,23.1248173253513,-53.0601653264822));
#70609=CARTESIAN_POINT('Ctrl Pts',(-20.8402433271325,26.9811416361272,-52.8612784151072));
#70610=CARTESIAN_POINT('Ctrl Pts',(-24.9718422390485,27.6847697513548,-52.6623915037324));
#70611=CARTESIAN_POINT('Ctrl Pts',(-27.7971207408364,24.5891270909661,-52.4635045923575));
#70612=CARTESIAN_POINT('Ctrl Pts',(-26.7198874334676,20.5388467926438,-52.2646176809826));
#70613=CARTESIAN_POINT('Ctrl Pts',(-22.7300283920912,19.2557930434072,-52.0657307696078));
#70614=CARTESIAN_POINT('Ctrl Pts',(-19.4938857914712,21.9189834537864,-51.8668438582328));
#70615=CARTESIAN_POINT('Ctrl Pts',(-19.9852003019322,26.0811718379532,-51.6679569468579));
#70616=CARTESIAN_POINT('Ctrl Pts',(-23.7524955449617,27.9176599662382,-51.469070035483));
#70617=CARTESIAN_POINT('Ctrl Pts',(-27.333946606178,25.740870957263,-51.2701831241082));
#70618=CARTESIAN_POINT('Ctrl Pts',(-27.4385036172981,21.5510893490035,-51.0712962127331));
#70619=CARTESIAN_POINT('Ctrl Pts',(-23.9700875500751,19.198369204551,-50.8724093013584));
#70620=CARTESIAN_POINT('Ctrl Pts',(-20.1158786970995,20.8446608588845,-50.6735223899835));
#70621=CARTESIAN_POINT('Ctrl Pts',(-19.4175682112343,24.9771618641855,-50.4746354786085));
#70622=CARTESIAN_POINT('Ctrl Pts',(-22.516844222024,27.7984541748875,-50.2757485672338));
#70623=CARTESIAN_POINT('Ctrl Pts',(-26.565734850825,26.7160093635963,-50.0768616558588));
#70624=CARTESIAN_POINT('Ctrl Pts',(-27.8436528990832,22.7245024357032,-49.8779747444839));
#70625=CARTESIAN_POINT('Ctrl Pts',(-25.1763000300321,19.4917898339631,-49.6790878331089));
#70626=CARTESIAN_POINT('Ctrl Pts',(-21.0147473761012,19.9884603505462,-49.4802009217342));
#70627=CARTESIAN_POINT('Ctrl Pts',(-19.1831089847741,23.7581158914279,-49.2813140103592));
#70628=CARTESIAN_POINT('Ctrl Pts',(-21.3645052403547,27.3367626286208,-49.0824270989844));
#70629=CARTESIAN_POINT('Ctrl Pts',(-25.5544179358669,27.4359276298519,-48.8835401876094));
#70630=CARTESIAN_POINT('Ctrl Pts',(-27.9026725501486,23.9644866667952,-48.6846532762346));
#70631=CARTESIAN_POINT('Ctrl Pts',(-26.2514221918332,20.1123996548436,-48.4857663648597));
#70632=CARTESIAN_POINT('Ctrl Pts',(-22.1180259372698,19.4194079548613,-48.2868794534847));
#70633=CARTESIAN_POINT('Ctrl Pts',(-19.3007244901924,22.5223121831255,-48.08799254211));
#70634=CARTESIAN_POINT('Ctrl Pts',(-20.3883790126936,26.5698064367551,-47.8891056307349));
#70635=CARTESIAN_POINT('Ctrl Pts',(-24.381527216491,27.842586667586,-47.6902187193602));
#70636=CARTESIAN_POINT('Ctrl Pts',(-27.6108044654305,25.1710757574519,-47.4913318079851));
#70637=CARTESIAN_POINT('Ctrl Pts',(-27.1087787652961,21.010165725994,-47.2924448966104));
#70638=CARTESIAN_POINT('Ctrl Pts',(-23.3367691697513,19.1833801051285,-47.0935579852354));
#70639=CARTESIAN_POINT('Ctrl Pts',(-19.7609326834278,21.3693799945523,-46.8946710738606));
#70640=CARTESIAN_POINT('Ctrl Pts',(-19.6671598563197,25.5594168381109,-46.6957841624856));
#70641=CARTESIAN_POINT('Ctrl Pts',(-23.141619965915,27.9032020331139,-46.4968972511108));
#70642=CARTESIAN_POINT('Ctrl Pts',(-26.9915787571332,26.2469957055673,-46.2980103397358));
#70643=CARTESIAN_POINT('Ctrl Pts',(-27.6792505235205,22.1127110473469,-46.099123428361));
#70644=CARTESIAN_POINT('Ctrl Pts',(-24.572723216718,19.2994051298232,-45.900236516986));
#70645=CARTESIAN_POINT('Ctrl Pts',(-20.5266320415966,20.3922675621942,-45.7013496056113));
#70646=CARTESIAN_POINT('Ctrl Pts',(-19.2589917361332,24.3870504285648,-45.5024626942362));
#70647=CARTESIAN_POINT('Ctrl Pts',(-21.9346562628749,27.6128869764729,-45.3035757828615));
#70648=CARTESIAN_POINT('Ctrl Pts',(-26.0949167806869,27.105506924227,-45.1046888714865));
#70649=CARTESIAN_POINT('Ctrl Pts',(-27.9168466056238,23.3311495211067,-44.9058019601116));
#70650=CARTESIAN_POINT('Ctrl Pts',(-25.7262467027435,19.7581292078445,-44.7069150487368));
#70651=CARTESIAN_POINT('Ctrl Pts',(-21.5360926505501,19.6697487101633,-44.5080281373618));
#70652=CARTESIAN_POINT('Ctrl Pts',(-19.1967807565319,23.1472222120017,-44.309141225987));
#70653=CARTESIAN_POINT('Ctrl Pts',(-20.8579403103511,26.9950464063015,-44.110254314612));
#70654=CARTESIAN_POINT('Ctrl Pts',(-24.9931065251517,27.677397100193,-43.9113674032373));
#70655=CARTESIAN_POINT('Ctrl Pts',(-27.8024122538098,24.5672518597881,-43.7124804918622));
#70656=CARTESIAN_POINT('Ctrl Pts',(-26.7043437215347,20.5225704641884,-43.5135935804875));
#70657=CARTESIAN_POINT('Ctrl Pts',(-22.707932808629,19.2600721835198,-43.3147066691125));
#70658=CARTESIAN_POINT('Ctrl Pts',(-19.4855423042849,21.9398858955148,-43.1158197577376));
#70659=CARTESIAN_POINT('Ctrl Pts',(-19.998275868335,26.0994900095838,-42.9169328463627));
#70660=CARTESIAN_POINT('Ctrl Pts',(-23.7749748280544,27.9165610211672,-42.7180459349879));
#70661=CARTESIAN_POINT('Ctrl Pts',(-27.3451730507276,25.7213647328356,-42.5191590236129));
#70662=CARTESIAN_POINT('Ctrl Pts',(-27.4281610726089,21.5311004116133,-42.3202721122381));
#70663=CARTESIAN_POINT('Ctrl Pts',(-23.9476799378133,19.1962656928772,-42.1213852008632));
#70664=CARTESIAN_POINT('Ctrl Pts',(-20.1019967130816,20.8623757218069,-41.9224982894882));
#70665=CARTESIAN_POINT('Ctrl Pts',(-19.4249682217745,24.9984166446511,-41.7236113781134));
#70666=CARTESIAN_POINT('Ctrl Pts',(-22.5387262448534,27.8037175317566,-41.5247244667385));
#70667=CARTESIAN_POINT('Ctrl Pts',(-26.5819911622529,26.7004447181652,-41.3258375553636));
#70668=CARTESIAN_POINT('Ctrl Pts',(-27.8393453272154,22.7024123774587,-41.1269506439887));
#70669=CARTESIAN_POINT('Ctrl Pts',(-25.1553868681933,19.483473253504,-40.9280637326138));
#70670=CARTESIAN_POINT('Ctrl Pts',(-20.9964460468774,20.0015594801844,-40.729176821239));
#70671=CARTESIAN_POINT('Ctrl Pts',(-19.1842368580253,23.780593741649,-40.530289909864));
#70672=CARTESIAN_POINT('Ctrl Pts',(-21.3840258961909,27.3479639608791,-40.3314029984892));
#70673=CARTESIAN_POINT('Ctrl Pts',(-25.5743935466533,27.4255593695183,-40.1325160871142));
#70674=CARTESIAN_POINT('Ctrl Pts',(-27.904747223225,23.9420763660328,-39.9336291757394));
#70675=CARTESIAN_POINT('Ctrl Pts',(-26.2336894785457,20.0985404799728,-39.7347422643644));
#70676=CARTESIAN_POINT('Ctrl Pts',(-22.0967806976434,19.4268353125242,-39.5358553529896));
#70677=CARTESIAN_POINT('Ctrl Pts',(-19.2954892981446,22.5442009613658,-39.3369684416147));
#70678=CARTESIAN_POINT('Ctrl Pts',(-20.4039645658452,26.5860427042324,-39.1380815302399));
#70679=CARTESIAN_POINT('Ctrl Pts',(-24.4036117129327,27.8382506710969,-38.9391946188649));
#70680=CARTESIAN_POINT('Ctrl Pts',(-27.6190941253889,25.1501519101382,-38.7403077074901));
#70681=CARTESIAN_POINT('Ctrl Pts',(-27.0956560941167,20.9918812694871,-38.5414207961151));
#70682=CARTESIAN_POINT('Ctrl Pts',(-23.314292789629,19.184536904692,-38.3425338847403));
#70683=CARTESIAN_POINT('Ctrl Pts',(-19.7497564820121,21.3889150494678,-38.1436469733653));
#70684=CARTESIAN_POINT('Ctrl Pts',(-19.6775538151261,25.5793790892106,-37.9447600619905));
#70685=CARTESIAN_POINT('Ctrl Pts',(-23.1640329180628,27.9052478641569,-37.7458731506156));
#70686=CARTESIAN_POINT('Ctrl Pts',(-27.0054150999034,26.229245171283,-37.5469862392407));
#70687=CARTESIAN_POINT('Ctrl Pts',(-27.6717958310359,22.0914753837455,-37.3480993278658));
#70688=CARTESIAN_POINT('Ctrl Pts',(-24.5508277193181,19.294198111267,-37.1492124164908));
#70689=CARTESIAN_POINT('Ctrl Pts',(-20.5104158449599,20.4078739972541,-36.9503255051161));
#70690=CARTESIAN_POINT('Ctrl Pts',(-19.2633561500621,24.409129326628,-36.7514385937411));
#70691=CARTESIAN_POINT('Ctrl Pts',(-21.95559076101,27.6211497022014,-36.5525516823663));
#70692=CARTESIAN_POINT('Ctrl Pts',(-26.1131843341947,27.0923607332398,-36.3536647709913));
#70693=CARTESIAN_POINT('Ctrl Pts',(-27.9156608816637,23.3086746483078,-36.1547778596165));
#70694=CARTESIAN_POINT('Ctrl Pts',(-25.7066972811022,19.7469781557811,-35.9558909482416));
#70695=CARTESIAN_POINT('Ctrl Pts',(-21.5161437921982,19.6801683502284,-35.7570040368667));
#70696=CARTESIAN_POINT('Ctrl Pts',(-19.1947637709106,23.1696377784152,-35.5581171254918));
#70697=CARTESIAN_POINT('Ctrl Pts',(-20.8757086362342,27.008859894056,-35.3592302141169));
#70698=CARTESIAN_POINT('Ctrl Pts',(-25.0143325775584,27.6699150852328,-35.160343302742));
#70699=CARTESIAN_POINT('Ctrl Pts',(-27.8075910902507,24.5453496794914,-34.9614563913671));
#70700=CARTESIAN_POINT('Ctrl Pts',(-26.6887164304136,20.5063743652492,-34.7625694799922));
#70701=CARTESIAN_POINT('Ctrl Pts',(-22.6858595455104,19.2644650076606,-34.5636825686173));
#70702=CARTESIAN_POINT('Ctrl Pts',(-19.4773065264707,21.9608310098002,-34.3647956572424));
#70703=CARTESIAN_POINT('Ctrl Pts',(-20.0114455573576,26.1177406298384,-34.1659087458676));
#70704=CARTESIAN_POINT('Ctrl Pts',(-23.7974481563076,27.9153463747746,-33.9670218344926));
#70705=CARTESIAN_POINT('Ctrl Pts',(-27.3562989349707,25.7018009768453,-33.7681349231178));
#70706=CARTESIAN_POINT('Ctrl Pts',(-27.4177157685418,21.5111649790478,-33.5692480117429));
#70707=CARTESIAN_POINT('Ctrl Pts',(-23.9252617942581,19.1942775560179,-33.370361100368));
#70708=CARTESIAN_POINT('Ctrl Pts',(-20.0882061032203,20.8801618098615,-33.1714741889931));
#70709=CARTESIAN_POINT('Ctrl Pts',(-19.4324775468188,25.019633050709,-32.9725872776182));
#70710=CARTESIAN_POINT('Ctrl Pts',(-22.5606350717733,27.8088681775051,-32.7737003662433));
#70711=CARTESIAN_POINT('Ctrl Pts',(-26.5981671366712,26.6847965968643,-32.5748134548684));
#70712=CARTESIAN_POINT('Ctrl Pts',(-27.8349241001381,22.680344785842,-32.3759265434936));
#70713=CARTESIAN_POINT('Ctrl Pts',(-25.1344311724462,19.475264437244,-32.1770396321186));
#70714=CARTESIAN_POINT('Ctrl Pts',(-20.9782123901021,20.0147526454313,-31.9781527207438));
#70715=CARTESIAN_POINT('Ctrl Pts',(-19.1854804248391,23.8030654881368,-31.7792658093688));
#70716=CARTESIAN_POINT('Ctrl Pts',(-21.403603954129,27.3590646588755,-31.580378897994));
#70717=CARTESIAN_POINT('Ctrl Pts',(-25.5943155204161,27.4150884187485,-31.381491986619));
#70718=CARTESIAN_POINT('Ctrl Pts',(-27.9067065080293,23.9196556824641,-31.1826050752442));
#70719=CARTESIAN_POINT('Ctrl Pts',(-26.2158856577764,20.0847727708444,-30.9837181638693));
#70720=CARTESIAN_POINT('Ctrl Pts',(-22.0755739730722,19.4343719352159,-30.7848312524944));
#70721=CARTESIAN_POINT('Ctrl Pts',(-19.2903668516188,22.5661163986241,-30.5859443411196));
#70722=CARTESIAN_POINT('Ctrl Pts',(-20.4196334914102,26.6021985273398,-30.3870574297446));
#70723=CARTESIAN_POINT('Ctrl Pts',(-24.4256735965,27.8338010484055,-30.1881705183698));
#70724=CARTESIAN_POINT('Ctrl Pts',(-27.6272759664994,25.1291856676358,-29.9892836069948));
#70725=CARTESIAN_POINT('Ctrl Pts',(-27.0824394744957,20.9736646063891,-29.79039669562));
#70726=CARTESIAN_POINT('Ctrl Pts',(-23.2918226621234,19.1858093898673,-29.591509784245));
#70727=CARTESIAN_POINT('Ctrl Pts',(-19.7386809886471,21.4085073769292,-29.3926228728702));
#70728=CARTESIAN_POINT('Ctrl Pts',(-19.6880503952571,25.5992875711766,-29.1937359614953));
#70729=CARTESIAN_POINT('Ctrl Pts',(-23.1864561045126,27.9071782936616,-28.9948490501204));
#70730=CARTESIAN_POINT('Ctrl Pts',(-27.0191598854974,26.2114236472851,-28.7959621387456));
#70731=CARTESIAN_POINT('Ctrl Pts',(-27.6642319231788,22.0702783757829,-28.5970752273706));
#70732=CARTESIAN_POINT('Ctrl Pts',(-24.528905708017,19.2891038724476,-28.3981883159958));
#70733=CARTESIAN_POINT('Ctrl Pts',(-20.4942801999204,20.4235637011325,-28.1993014046208));
#70734=CARTESIAN_POINT('Ctrl Pts',(-19.2678341609985,24.4311854656078,-28.000414493246));
#70735=CARTESIAN_POINT('Ctrl Pts',(-21.9765675155443,27.6293045546121,-27.801527581871));
#70736=CARTESIAN_POINT('Ctrl Pts',(-26.1313839734455,27.0791206811336,-27.6026406704962));
#70737=CARTESIAN_POINT('Ctrl Pts',(-27.9143594802346,23.2862061769991,-27.4037537591212));
#70738=CARTESIAN_POINT('Ctrl Pts',(-25.6870907165655,19.7359278853903,-27.2048668477464));
#70739=CARTESIAN_POINT('Ctrl Pts',(-21.4962488350009,19.6906905423363,-27.0059799363715));
#70740=CARTESIAN_POINT('Ctrl Pts',(-19.1928621999026,23.1920634306094,-26.8070930249966));
#70741=CARTESIAN_POINT('Ctrl Pts',(-20.8935478339452,27.0225817333519,-26.6082061136217));
#70742=CARTESIAN_POINT('Ctrl Pts',(-25.0355198338064,27.6623239047374,-26.4093192022468));
#70743=CARTESIAN_POINT('Ctrl Pts',(-27.8126571129269,24.5234211304542,-26.2104322908719));
#70744=CARTESIAN_POINT('Ctrl Pts',(-26.6730059742064,20.4902589250009,-26.011545379497));
#70745=CARTESIAN_POINT('Ctrl Pts',(-22.6638091876472,19.2689713994255,-25.8126584681222));
#70746=CARTESIAN_POINT('Ctrl Pts',(-19.4691786762658,21.9818182416253,-25.6137715567472));
#70747=CARTESIAN_POINT('Ctrl Pts',(-20.024709020021,26.1359232151003,-25.4148846453724));
#70748=CARTESIAN_POINT('Ctrl Pts',(-23.8199149342081,27.9140160592465,-25.2159977339975));
#70749=CARTESIAN_POINT('Ctrl Pts',(-27.367323964086,25.6821802077056,-25.0171108226226));
#70750=CARTESIAN_POINT('Ctrl Pts',(-27.4071679818835,21.4912835795687,-24.8182239112477));
#70751=CARTESIAN_POINT('Ctrl Pts',(-23.9028337134602,19.1924048466563,-24.6193369998728));
#70752=CARTESIAN_POINT('Ctrl Pts',(-20.0745072329483,20.8980186517408,-24.4204500884979));
#70753=CARTESIAN_POINT('Ctrl Pts',(-19.4400959873801,25.0408105201528,-24.2215631771231));
#70754=CARTESIAN_POINT('Ctrl Pts',(-22.5825701222292,27.8139059756478,-24.0226762657481));
#70755=CARTESIAN_POINT('Ctrl Pts',(-26.6142623454384,26.6690654143477,-23.8237893543733));
#70756=CARTESIAN_POINT('Ctrl Pts',(-27.8303893350082,22.6583002456145,-23.6249024429983));
#70757=CARTESIAN_POINT('Ctrl Pts',(-25.1134334980889,19.4671636027058,-23.4260155316235));
#70758=CARTESIAN_POINT('Ctrl Pts',(-20.9600468889425,20.0280394966856,-23.2271286202485));
#70759=CARTESIAN_POINT('Ctrl Pts',(-19.1868396522625,23.8255305354201,-23.0282417088737));
#70760=CARTESIAN_POINT('Ctrl Pts',(-21.4232388953766,27.3700644284562,-22.8293547974988));
#70761=CARTESIAN_POINT('Ctrl Pts',(-25.6141833292499,27.4045150550087,-22.6304678861239));
#70762=CARTESIAN_POINT('Ctrl Pts',(-27.9085503526435,23.8972252102072,-22.431580974749));
#70763=CARTESIAN_POINT('Ctrl Pts',(-26.1980112013026,20.0710968922841,-22.2326940633741));
#70764=CARTESIAN_POINT('Ctrl Pts',(-22.0544063255061,19.4420176232257,-22.0338071519992));
#70765=CARTESIAN_POINT('Ctrl Pts',(-19.2853572863529,22.5880579141706,-21.8349202406243));
#70766=CARTESIAN_POINT('Ctrl Pts',(-20.4353853741828,26.6182734779693,-21.6360333292494));
#70767=CARTESIAN_POINT('Ctrl Pts',(-24.4477122825825,27.8292379174207,-21.4371464178746));
#70768=CARTESIAN_POINT('Ctrl Pts',(-27.6353497719544,25.1081775855218,-21.2382595064997));
#70769=CARTESIAN_POINT('Ctrl Pts',(-27.0691292566558,20.9555162194172,-21.0393725951248));
#70770=CARTESIAN_POINT('Ctrl Pts',(-23.2693593826632,19.1871975269351,-20.8404856837499));
#70771=CARTESIAN_POINT('Ctrl Pts',(-19.7277064968184,21.428156457766,-20.641598772375));
#70772=CARTESIAN_POINT('Ctrl Pts',(-19.6986493185672,25.6191417564607,-20.4427118610002));
#70773=CARTESIAN_POINT('Ctrl Pts',(-23.2088889310798,27.9089932704743,-20.2438249496252));
#70774=CARTESIAN_POINT('Ctrl Pts',(-27.0328127496967,26.1935316058201,-20.0449380382504));
#70775=CARTESIAN_POINT('Ctrl Pts',(-27.6565590003829,22.0491205851516,-19.8460511268754));
#70776=CARTESIAN_POINT('Ctrl Pts',(-24.5069577637188,19.2841225483553,-19.6471642155006));
#70777=CARTESIAN_POINT('Ctrl Pts',(-20.4782255340512,20.4393362580734,-19.4482773041257));
#70778=CARTESIAN_POINT('Ctrl Pts',(-19.2724256502808,24.4532182610454,-19.2493903927508));
#70779=CARTESIAN_POINT('Ctrl Pts',(-21.9975859706218,27.6373513176123,-19.0505034813759));
#70780=CARTESIAN_POINT('Ctrl Pts',(-26.1495152161732,27.0657871187522,-18.851616570001));
#70781=CARTESIAN_POINT('Ctrl Pts',(-27.9129424358214,23.2637447025648,-18.6527296586261));
#70782=CARTESIAN_POINT('Ctrl Pts',(-25.6674275286819,19.7249786894894,-18.4538427472512));
#70783=CARTESIAN_POINT('Ctrl Pts',(-21.4764083061483,19.7013150076628,-18.2549558358763));
#70784=CARTESIAN_POINT('Ctrl Pts',(-19.1910760938974,23.2144985743345,-18.0560689245014));
#70785=CARTESIAN_POINT('Ctrl Pts',(-20.9114574307693,27.0362115605785,-17.8571820131265));
#70786=CARTESIAN_POINT('Ctrl Pts',(-25.056667732462,27.6546237598632,-17.6582951017517));
#70787=CARTESIAN_POINT('Ctrl Pts',(-27.8176101875956,24.5014667937537,-17.4594081903767));
#70788=CARTESIAN_POINT('Ctrl Pts',(-26.6572127692192,20.4742245704813,-17.2605212790019));
#70789=CARTESIAN_POINT('Ctrl Pts',(-22.6417823193444,19.273591239401,-17.061634367627));
#70790=CARTESIAN_POINT('Ctrl Pts',(-19.461158969047,22.0028470348563,-16.8627474562521));
#70791=CARTESIAN_POINT('Ctrl Pts',(-20.0380659048616,26.1540372835553,-16.6638605448772));
#70792=CARTESIAN_POINT('Ctrl Pts',(-23.8423745664162,27.9125701098348,-16.4649736335023));
#70793=CARTESIAN_POINT('Ctrl Pts',(-27.3782478459255,25.6625029453405,-16.2660867221274));
#70794=CARTESIAN_POINT('Ctrl Pts',(-27.3965179921361,21.4714567400069,-16.0671998107525));
#70795=CARTESIAN_POINT('Ctrl Pts',(-23.8803962897337,19.1906476144163,-15.8683128993776));
#70796=CARTESIAN_POINT('Ctrl Pts',(-20.0609004652675,20.9159457742625,-15.6694259880027));
#70797=CARTESIAN_POINT('Ctrl Pts',(-19.44782334158,25.0619484918082,-15.4705390766279));
#70798=CARTESIAN_POINT('Ctrl Pts',(-22.6045308149718,27.8188307926899,-15.271652165253));
#70799=CARTESIAN_POINT('Ctrl Pts',(-26.6302763620529,26.6532515874704,-15.0727652538781));
#70800=CARTESIAN_POINT('Ctrl Pts',(-27.8257411519907,22.6362793409266,-14.8738783425032));
#70801=CARTESIAN_POINT('Ctrl Pts',(-25.0923944015314,19.4591709645508,-14.6749914311283));
#70802=CARTESIAN_POINT('Ctrl Pts',(-20.9419500247604,20.0414196818637,-14.4761045197534));
#70803=CARTESIAN_POINT('Ctrl Pts',(-19.1883145042778,23.8479882882055,-14.2772176083785));
#70804=CARTESIAN_POINT('Ctrl Pts',(-21.4429301996344,27.3809629781424,-14.0783306970036));
#70805=CARTESIAN_POINT('Ctrl Pts',(-25.6339964466844,27.3938395584788,-13.8794437856287));
#70806=CARTESIAN_POINT('Ctrl Pts',(-27.9102787082077,23.8747855436392,-13.6805568742538));
#70807=CARTESIAN_POINT('Ctrl Pts',(-26.1800665827734,20.0575132066841,-13.4816699628789));
#70808=CARTESIAN_POINT('Ctrl Pts',(-22.033278315859,19.4497721739535,-13.2827830515041));
#70809=CARTESIAN_POINT('Ctrl Pts',(-19.2804607350937,22.6100249265848,-13.0838961401291));
#70810=CARTESIAN_POINT('Ctrl Pts',(-20.4512197967597,26.6342671301568,-12.8850092287543));
#70811=CARTESIAN_POINT('Ctrl Pts',(-24.4697271871847,27.8245613990593,-12.6861223173794));
#70812=CARTESIAN_POINT('Ctrl Pts',(-27.6433153278088,25.0871282204823,-12.4872354060045));
#70813=CARTESIAN_POINT('Ctrl Pts',(-27.0557257932998,20.9374365894791,-12.2883484946296));
#70814=CARTESIAN_POINT('Ctrl Pts',(-23.2469035464947,19.1887012791116,-12.0894615832547));
#70815=CARTESIAN_POINT('Ctrl Pts',(-19.7168332973353,21.4478617713041,-11.8905746718798));
#70816=CARTESIAN_POINT('Ctrl Pts',(-19.7093503041991,25.638941118954,-11.6916877605049));
#70817=CARTESIAN_POINT('Ctrl Pts',(-23.2313308033251,27.9106927465004,-11.49280084913));
#70818=CARTESIAN_POINT('Ctrl Pts',(-27.0463733307188,26.175569521003,-11.2939139377551));
#70819=CARTESIAN_POINT('Ctrl Pts',(-27.6487772659703,22.0280025725045,-11.0950270263803));
#70820=CARTESIAN_POINT('Ctrl Pts',(-24.4849844680144,19.2792542709887,-10.8961401150054));
#70821=CARTESIAN_POINT('Ctrl Pts',(-20.4622522727791,20.4551912501253,-10.6972532036305));
#70822=CARTESIAN_POINT('Ctrl Pts',(-19.2771304962409,24.4752271291019,-10.4983662922556));
#70823=CARTESIAN_POINT('Ctrl Pts',(-22.0186455692821,27.6452897779736,-10.2994793808807));
#70824=CARTESIAN_POINT('Ctrl Pts',(-26.1675775819241,27.0523603994167,-10.1005924695058));
#70825=CARTESIAN_POINT('Ctrl Pts',(-27.9114097859742,23.2412908202039,-9.90170555813094));
#70826=CARTESIAN_POINT('Ctrl Pts',(-25.6477082384987,19.7141308582173,-9.70281864675604));
#70827=CARTESIAN_POINT('Ctrl Pts',(-21.4566227313875,19.7120414646744,-9.50393173538115));
#70828=CARTESIAN_POINT('Ctrl Pts',(-19.1894055002238,23.2369426150895,-9.30504482400626));
#70829=CARTESIAN_POINT('Ctrl Pts',(-20.9294369521262,27.0497490145641,-9.10615791263137));
#70830=CARTESIAN_POINT('Ctrl Pts',(-25.0777757131341,27.6468148546534,-8.90727100125649));
#70831=CARTESIAN_POINT('Ctrl Pts',(-27.822450183007,24.4794872511504,-8.70838408988158));
#70832=CARTESIAN_POINT('Ctrl Pts',(-26.6413372339507,20.4582717265789,-8.5094971785067));
#70833=CARTESIAN_POINT('Ctrl Pts',(-22.6197795242843,19.2783244051677,-8.3106102671318));
#70834=CARTESIAN_POINT('Ctrl Pts',(-19.4532476173261,22.0239168322588,-8.11172335575693));
#70835=CARTESIAN_POINT('Ctrl Pts',(-20.0515158579395,26.1720823552048,-7.91283644438202));
#70836=CARTESIAN_POINT('Ctrl Pts',(-23.8648264577823,27.9110085648553,-7.71394953300715));
#70837=CARTESIAN_POINT('Ctrl Pts',(-27.3890702910207,25.6427697111708,-7.51506262163224));
#70838=CARTESIAN_POINT('Ctrl Pts',(-27.3857660815101,21.4516849857467,-7.31617571025736));
#70839=CARTESIAN_POINT('Ctrl Pts',(-23.8579501176399,19.1890059058624,-7.11728879888246));
#70840=CARTESIAN_POINT('Ctrl Pts',(-20.0473861607387,20.9339427023821,-6.91840188750758));
#70841=CARTESIAN_POINT('Ctrl Pts',(-19.455659404654,25.083046405547,-6.71951497613268));
#70842=CARTESIAN_POINT('Ctrl Pts',(-22.6265165680722,27.8236424981302,-6.52062806475779));
#70843=CARTESIAN_POINT('Ctrl Pts',(-26.6462087621649,26.6373555352779,-6.32174115338291));
#70844=CARTESIAN_POINT('Ctrl Pts',(-27.8209796742559,22.6142826553032,-6.12285424200801));
#70845=CARTESIAN_POINT('Ctrl Pts',(-25.0713144402817,19.451286734573,-5.92396733063314));
#70846=CARTESIAN_POINT('Ctrl Pts',(-20.9239222770979,20.0548928464088,-5.72508041925822));
#70847=CARTESIAN_POINT('Ctrl Pts',(-19.1899049418037,23.8704381513923,-5.52619350788335));
#70848=CARTESIAN_POINT('Ctrl Pts',(-21.462677345109,27.391760019137,-5.32730659650845));
#70849=CARTESIAN_POINT('Ctrl Pts',(-25.6537543476985,27.3830622120451,-5.12841968513356));
#70850=CARTESIAN_POINT('Ctrl Pts',(-27.9118915289232,23.8523372773817,-4.92953277375868));
#70851=CARTESIAN_POINT('Ctrl Pts',(-26.1620522776973,20.044022073994,-4.73064586238378));
#70852=CARTESIAN_POINT('Ctrl Pts',(-22.0121905039951,19.4576353819139,-4.53175895100889));
#70853=CARTESIAN_POINT('Ctrl Pts',(-19.2756773275934,22.6320168537699,-4.332872039634));
#70854=CARTESIAN_POINT('Ctrl Pts',(-20.4671363395497,26.6501790600916,-4.13398512825911));
#70855=CARTESIAN_POINT('Ctrl Pts',(-24.4917177269413,27.8197716172427,-3.93509821688421));
#70856=CARTESIAN_POINT('Ctrl Pts',(-27.6511724229859,25.0660381302974,-3.73621130550934));
#70857=CARTESIAN_POINT('Ctrl Pts',(-27.0422294396017,20.9194261956609,-3.53732439413444));
#70858=CARTESIAN_POINT('Ctrl Pts',(-23.2244557486677,19.1903206065495,-3.33843748275955));
#70859=CARTESIAN_POINT('Ctrl Pts',(-19.7060616783232,21.4676227953791,-3.13955057138466));
#70860=CARTESIAN_POINT('Ctrl Pts',(-19.7201530685912,25.6586851339996,-2.94066366000977));
#70861=CARTESIAN_POINT('Ctrl Pts',(-23.2537811265686,27.9122766767063,-2.74177674863487));
#70862=CARTESIAN_POINT('Ctrl Pts',(-27.0598412692263,26.157537868805,-2.54288983726));
#70863=CARTESIAN_POINT('Ctrl Pts',(-27.6408869261465,22.0069248974407,-2.34400292588509));
#70864=CARTESIAN_POINT('Ctrl Pts',(-24.4629864031666,19.2744991693506,-2.14511601451021));
#70865=CARTESIAN_POINT('Ctrl Pts',(-20.4463608393743,20.4711282571522,-1.94622910313531));
#70866=CARTESIAN_POINT('Ctrl Pts',(-19.2819485742067,24.4972114865714,-1.74734219176043));
#70867=CARTESIAN_POINT('Ctrl Pts',(-22.0397457534735,27.6531197253375,-1.54845528038553));
#70868=CARTESIAN_POINT('Ctrl Pts',(-26.18557059207,27.0388408789175,-1.34956836901064));
#70869=CARTESIAN_POINT('Ctrl Pts',(-27.909761571306,23.2188451249141,-1.15068145763575));
#70870=CARTESIAN_POINT('Ctrl Pts',(-25.627933368551,19.7033846790271,-0.951794546260857));
#70871=CARTESIAN_POINT('Ctrl Pts',(-21.4368926350098,19.7228696291338,-0.752907634885971));
#70872=CARTESIAN_POINT('Ctrl Pts',(-19.1878504631509,23.2593949581373,-0.554020723511071));
#70873=CARTESIAN_POINT('Ctrl Pts',(-20.9474859215826,27.0631937365842,-0.355133812136187));
#70874=CARTESIAN_POINT('Ctrl Pts',(-25.0988432164898,27.6388973960336,-0.15624690076129));
#70875=CARTESIAN_POINT('Ctrl Pts',(-27.8271769709077,24.4574830850727,0.0426400106135906));
#70876=CARTESIAN_POINT('Ctrl Pts',(-26.6253797890813,20.442400816023,0.241526921988483));
#70877=CARTESIAN_POINT('Ctrl Pts',(-22.5978013855116,19.2831707713033,0.440413833363379));
#70878=CARTESIAN_POINT('Ctrl Pts',(-19.4454448307434,22.0450270755113,0.63930074473826));
#70879=CARTESIAN_POINT('Ctrl Pts',(-20.0650585228489,26.1900579518786,0.838187656113157));
#70880=CARTESIAN_POINT('Ctrl Pts',(-23.887270013361,27.9093314656867,1.03707456748805));
#70881=CARTESIAN_POINT('Ctrl Pts',(-27.3997910125914,25.6229810281009,1.23596147886293));
#70882=CARTESIAN_POINT('Ctrl Pts',(-27.3749125349168,21.4319688407133,1.43484839023782));
#70883=CARTESIAN_POINT('Ctrl Pts',(-23.8354957919727,19.1874797644976,1.63373530161272));
#70884=CARTESIAN_POINT('Ctrl Pts',(-20.033964677473,20.9520089592048,1.8326222129876));
#70885=CARTESIAN_POINT('Ctrl Pts',(-19.4636039689568,25.1041037023031,2.0315091243625));
#70886=CARTESIAN_POINT('Ctrl Pts',(-22.6485267989372,27.8283409644652,2.23039603573739));
#70887=CARTESIAN_POINT('Ctrl Pts',(-26.662059123587,26.6213776789941,2.42928294711228));
#70888=CARTESIAN_POINT('Ctrl Pts',(-27.8161050279772,22.5923107716267,2.62816985848716));
#70889=CARTESIAN_POINT('Ctrl Pts',(-25.0501941729305,19.4435111216939,2.82705676986206));
#70890=CARTESIAN_POINT('Ctrl Pts',(-20.9059641236666,20.0684586332996,3.02594368123694));
#70891=CARTESIAN_POINT('Ctrl Pts',(-19.1916109226953,23.8928795300895,3.22483059261183));
#70892=CARTESIAN_POINT('Ctrl Pts',(-21.4824798085275,27.4024552653329,3.42371750398671));
#70893=CARTESIAN_POINT('Ctrl Pts',(-25.6734565087343,27.3721833012931,3.62260441536165));
#70894=CARTESIAN_POINT('Ctrl Pts',(-27.9133887720521,23.8298810062832,3.82149132673651));
#70895=CARTESIAN_POINT('Ctrl Pts',(-26.1439687634292,20.030623851711,4.02037823811141));
#70896=CARTESIAN_POINT('Ctrl Pts',(-21.9911434487132,19.4656070387423,4.21926514948628));
#70897=CARTESIAN_POINT('Ctrl Pts',(-19.2710071906058,22.6540331129696,4.41815206086118));
#70898=CARTESIAN_POINT('Ctrl Pts',(-20.4831345807856,26.666008846129,4.61703897223605));
#70899=CARTESIAN_POINT('Ctrl Pts',(-24.5136833191324,27.814868698894,4.815925883611));
#70900=CARTESIAN_POINT('Ctrl Pts',(-27.6589208492834,25.044907873826,5.01481279498585));
#70901=CARTESIAN_POINT('Ctrl Pts',(-27.0286405531965,20.9014855152137,5.21369970636075));
#70902=CARTESIAN_POINT('Ctrl Pts',(-23.2020165840186,19.1920554663387,5.41258661773564));
#70903=CARTESIAN_POINT('Ctrl Pts',(-19.6953919252152,21.4874390063501,5.61147352911051));
#70904=CARTESIAN_POINT('Ctrl Pts',(-19.7310573254847,25.6783732784078,5.81036044048541));
#70905=CARTESIAN_POINT('Ctrl Pts',(-23.2762393059069,27.9137450191198,6.00924735186033));
#70906=CARTESIAN_POINT('Ctrl Pts',(-27.0732162083372,26.1394371270407,6.20813426323521));
#70907=CARTESIAN_POINT('Ctrl Pts',(-27.6328881899946,21.9858881184902,6.40702117461008));
#70908=CARTESIAN_POINT('Ctrl Pts',(-24.440964152095,19.2698573694446,6.605908085985));
#70909=CARTESIAN_POINT('Ctrl Pts',(-20.4305516549384,20.4871468568447,6.80479499735984));
#70910=CARTESIAN_POINT('Ctrl Pts',(-19.2868797565055,24.5191707508981,7.00368190873475));
#70911=CARTESIAN_POINT('Ctrl Pts',(-22.0608859640696,27.6608409522209,7.20256882010963));
#70912=CARTESIAN_POINT('Ctrl Pts',(-26.2034937698199,27.0252289155038,7.40145573148457));
#70913=CARTESIAN_POINT('Ctrl Pts',(-27.9079978354924,23.1964082114763,7.60034264285942));
#70914=CARTESIAN_POINT('Ctrl Pts',(-25.6081034428465,19.6927404366781,7.79922955423434));
#70915=CARTESIAN_POINT('Ctrl Pts',(-21.4172185398362,19.7337992141093,7.99811646560919));
#70916=CARTESIAN_POINT('Ctrl Pts',(-19.1864110238848,23.2818550085209,8.1970033769841));
#70917=CARTESIAN_POINT('Ctrl Pts',(-20.965603860865,27.0765453703715,8.39589028835899));
#70918=CARTESIAN_POINT('Ctrl Pts',(-25.1198696842683,27.6308715938061,8.5947771997339));
#70919=CARTESIAN_POINT('Ctrl Pts',(-27.8317904260442,24.4354548786015,8.79366411110879));
#70920=CARTESIAN_POINT('Ctrl Pts',(-26.609340857462,20.4266122593714,8.99255102248365));
#70921=CARTESIAN_POINT('Ctrl Pts',(-22.5758484854174,19.2881302093852,9.19143793385857));
#70922=CARTESIAN_POINT('Ctrl Pts',(-19.4377508160619,22.0661772052205,9.39032484523341));
#70923=CARTESIAN_POINT('Ctrl Pts',(-20.0786935407278,26.2079635972476,9.58921175660836));
#70924=CARTESIAN_POINT('Ctrl Pts',(-23.9097046384281,27.9075388567697,9.78809866798321));
#70925=CARTESIAN_POINT('Ctrl Pts',(-27.4104097265529,25.6031374205046,9.98698557935814));
#70926=CARTESIAN_POINT('Ctrl Pts',(-27.3639576399603,21.4123088273581,10.185872490733));
#70927=CARTESIAN_POINT('Ctrl Pts',(-23.8130339077415,19.1860692307627,10.3847594021079));
#70928=CARTESIAN_POINT('Ctrl Pts',(-20.0206363711217,20.9701440659991,10.5836463134828));
#70929=CARTESIAN_POINT('Ctrl Pts',(-19.4716568239683,25.1251198240861,10.7825332248577));
#70930=CARTESIAN_POINT('Ctrl Pts',(-22.6705609243254,27.8329260671917,10.9814201362326));
#70931=CARTESIAN_POINT('Ctrl Pts',(-26.6778270263059,26.605318442011,11.1803070476075));
#70932=CARTESIAN_POINT('Ctrl Pts',(-27.8111173423259,22.5703642721228,11.3791939589824));
#70933=CARTESIAN_POINT('Ctrl Pts',(-25.0290341591364,19.4358443319569,11.5780808703573));
#70934=CARTESIAN_POINT('Ctrl Pts',(-20.8880760403332,20.0821166830615,11.7769677817321));
#70935=CARTESIAN_POINT('Ctrl Pts',(-19.1934324017466,23.9153118296306,11.975854693107));
#70936=CARTESIAN_POINT('Ctrl Pts',(-21.5023370651513,27.4130484333204,12.1747416044819));
#70937=CARTESIAN_POINT('Ctrl Pts',(-25.6931024077111,27.3612031144989,12.3736285158569));
#70938=CARTESIAN_POINT('Ctrl Pts',(-27.9147703979196,23.807417325405,12.5725154272317));
#70939=CARTESIAN_POINT('Ctrl Pts',(-26.1258165191579,20.0173188948697,12.7714023386066));
#70940=CARTESIAN_POINT('Ctrl Pts',(-21.9701377077319,19.4736869332006,12.9702892499815));
#70941=CARTESIAN_POINT('Ctrl Pts',(-19.2664504478831,22.6760731207826,13.1691761613564));
#70942=CARTESIAN_POINT('Ctrl Pts',(-20.4992140965357,26.6817560688007,13.3680630727313));
#70943=CARTESIAN_POINT('Ctrl Pts',(-24.5356233816989,27.8098527739337,13.5669499841062));
#70944=CARTESIAN_POINT('Ctrl Pts',(-27.6665604013785,25.0237380109917,13.7658368954811));
#70945=CARTESIAN_POINT('Ctrl Pts',(-27.0149594941717,20.8836150235418,13.9647238068559));
#70946=CARTESIAN_POINT('Ctrl Pts',(-23.1795866471555,19.1939058125079,14.1636107182308));
#70947=CARTESIAN_POINT('Ctrl Pts',(-19.6848243207457,21.5073098791143,14.3624976296057));
#70948=CARTESIAN_POINT('Ctrl Pts',(-19.7420627859315,25.6980050304689,14.5613845409806));
#70949=CARTESIAN_POINT('Ctrl Pts',(-23.2987047462283,27.9150977348318,14.7602714523555));
#70950=CARTESIAN_POINT('Ctrl Pts',(-27.0864977936333,26.1212677753556,14.9591583637304));
#70951=CARTESIAN_POINT('Ctrl Pts',(-27.6247812694709,21.9648927930996,15.1580452751053));
#70952=CARTESIAN_POINT('Ctrl Pts',(-24.4189182983592,19.2653289942726,15.3569321864802));
#70953=CARTESIAN_POINT('Ctrl Pts',(-20.4148251383938,20.5032466247312,15.555819097855));
#70954=CARTESIAN_POINT('Ctrl Pts',(-19.2919239124675,24.5411043401908,15.75470600923));
#70955=CARTESIAN_POINT('Ctrl Pts',(-22.0820656408832,27.6684532540214,15.9535929206049));
#70956=CARTESIAN_POINT('Ctrl Pts',(-26.2213466402339,27.0115248698742,16.1524798319797));
#70957=CARTESIAN_POINT('Ctrl Pts',(-27.90611862527,23.1739806744387,16.3513667433546));
#70958=CARTESIAN_POINT('Ctrl Pts',(-25.5882189868514,19.6821984132284,16.5502536547295));
#70959=CARTESIAN_POINT('Ctrl Pts',(-21.3976009672041,19.7448299299816,16.7491405661044));
#70960=CARTESIAN_POINT('Ctrl Pts',(-19.1850872205686,23.304322171079,16.9480274774793));
#70961=CARTESIAN_POINT('Ctrl Pts',(-20.9837902898725,27.0898035621258,17.1469143888542));
#70962=CARTESIAN_POINT('Ctrl Pts',(-25.1408545592962,27.6227376606435,17.3458013002291));
#70963=CARTESIAN_POINT('Ctrl Pts',(-27.8362904261661,24.4134032154548,17.544688211604));
#70964=CARTESIAN_POINT('Ctrl Pts',(-26.5932208641028,20.4109064749995,17.7435751229789));
#70965=CARTESIAN_POINT('Ctrl Pts',(-22.5539214057241,19.293202587995,17.9424620343537));
#70966=CARTESIAN_POINT('Ctrl Pts',(-19.4301657771629,22.0873666609364,18.1413489457287));
#70967=CARTESIAN_POINT('Ctrl Pts',(-20.092420550266,26.2257988168362,18.3402358571035));
#70968=CARTESIAN_POINT('Ctrl Pts',(-23.9321297384963,27.9056307856063,18.5391227684785));
#70969=CARTESIAN_POINT('Ctrl Pts',(-27.4209261515234,25.5832394142105,18.7380096798533));
#70970=CARTESIAN_POINT('Ctrl Pts',(-27.3529016869309,21.3927054666449,18.9368965912282));
#70971=CARTESIAN_POINT('Ctrl Pts',(-23.7905650601562,19.184774342035,19.1357835026031));
#70972=CARTESIAN_POINT('Ctrl Pts',(-20.007401594867,20.9883475422089,19.3346704139779));
#70973=CARTESIAN_POINT('Ctrl Pts',(-19.4798177562985,25.1460942139971,19.5335573253529));
#70974=CARTESIAN_POINT('Ctrl Pts',(-22.6926183603619,27.8373976848105,19.7324442367278));
#70975=CARTESIAN_POINT('Ctrl Pts',(-26.6935120524933,26.5891782498768,19.9313311481027));
#70976=CARTESIAN_POINT('Ctrl Pts',(-27.8060167494689,22.5484437383441,20.1302180594776));
#70977=CARTESIAN_POINT('Ctrl Pts',(-25.0078349596116,19.4282865685217,20.3291049708524));
#70978=CARTESIAN_POINT('Ctrl Pts',(-20.8702585011083,20.095866633774,20.5279918822274));
#70979=CARTESIAN_POINT('Ctrl Pts',(-19.1953693306909,23.9377344555896,20.7268787936022));
#70980=CARTESIAN_POINT('Ctrl Pts',(-21.5222485887897,27.4235392423947,20.9257657049771));
#70981=CARTESIAN_POINT('Ctrl Pts',(-25.7126915240386,27.3501219426233,21.124652616352));
#70982=CARTESIAN_POINT('Ctrl Pts',(-27.9160363699146,23.7849468300045,21.3235395277269));
#70983=CARTESIAN_POINT('Ctrl Pts',(-26.1075960258935,20.0041075560337,21.5224264391018));
#70984=CARTESIAN_POINT('Ctrl Pts',(-21.9491738376752,19.4818748511826,21.7213133504767));
#70985=CARTESIAN_POINT('Ctrl Pts',(-19.2620072201731,22.6981362931779,21.9202002618515));
#70986=CARTESIAN_POINT('Ctrl Pts',(-20.5153744607142,26.6974203108268,22.1190871732265));
#70987=CARTESIAN_POINT('Ctrl Pts',(-24.5575373332589,27.8047239752771,22.3179740846014));
#70988=CARTESIAN_POINT('Ctrl Pts',(-27.6740908768329,25.0025291027673,22.5168609959763));
#70989=CARTESIAN_POINT('Ctrl Pts',(-27.0011866250572,20.8658151941895,22.7157479073511));
#70990=CARTESIAN_POINT('Ctrl Pts',(-23.1571665324412,19.1958715960246,22.914634818726));
#70991=CARTESIAN_POINT('Ctrl Pts',(-19.6743591449424,21.5272348871214,23.1135217301009));
#70992=CARTESIAN_POINT('Ctrl Pts',(-19.7531691583009,25.7175798699656,23.3124086414758));
#70993=CARTESIAN_POINT('Ctrl Pts',(-23.3211768522295,27.9163347880016,23.5112955528507));
#70994=CARTESIAN_POINT('Ctrl Pts',(-27.099685673169,26.1030302952045,23.7101824642256));
#70995=CARTESIAN_POINT('Ctrl Pts',(-27.6165663794003,21.9439394776331,23.9090693756005));
#70996=CARTESIAN_POINT('Ctrl Pts',(-24.3968494261405,19.2609141637993,24.1079562869754));
#70997=CARTESIAN_POINT('Ctrl Pts',(-20.3991817064806,20.5194271342477,24.3068431983502));
#70998=CARTESIAN_POINT('Ctrl Pts',(-19.2970809084129,24.5630116731296,24.5057301097252));
#70999=CARTESIAN_POINT('Ctrl Pts',(-22.103284222713,27.6759564292301,24.7046170211));
#71000=CARTESIAN_POINT('Ctrl Pts',(-26.2391287301751,26.9977291047774,24.9035039324749));
#71001=CARTESIAN_POINT('Ctrl Pts',(-27.9041239905479,23.1515631088375,25.1023908438499));
#71002=CARTESIAN_POINT('Ctrl Pts',(-25.5682805272645,19.6717588866363,25.3012777552247));
#71003=CARTESIAN_POINT('Ctrl Pts',(-21.378040437354,19.7559614870787,25.5001646665996));
#71004=CARTESIAN_POINT('Ctrl Pts',(-19.1838790875238,23.3267958455017,25.6990515779745));
#71005=CARTESIAN_POINT('Ctrl Pts',(-21.0020447281196,27.102967969889,25.8979384893494));
#71006=CARTESIAN_POINT('Ctrl Pts',(-25.1617972828013,27.6144957943989,26.0968254007243));
#71007=CARTESIAN_POINT('Ctrl Pts',(-27.8406768571304,24.3913287133657,26.2957123120992));
#71008=CARTESIAN_POINT('Ctrl Pts',(-26.5770202265301,20.3952838160355,26.494599223474));
#71009=CARTESIAN_POINT('Ctrl Pts',(-22.5320207456567,19.2983878917809,26.693486134849));
#71010=CARTESIAN_POINT('Ctrl Pts',(-19.4226898806994,22.1085946563589,26.8923730462238));
#71011=CARTESIAN_POINT('Ctrl Pts',(-20.1062392525582,26.2435635625186,27.0912599575988));
#71012=CARTESIAN_POINT('Ctrl Pts',(-23.9545445968963,27.9036065012466,27.2901468689736));
#71013=CARTESIAN_POINT('Ctrl Pts',(-27.4313402400131,25.5632890499054,27.4890337803486));
#71014=CARTESIAN_POINT('Ctrl Pts',(-27.3417445322793,21.3731564203992,27.6879206917233));
#71015=CARTESIAN_POINT('Ctrl Pts',(-23.7680906688437,19.1836005284276,27.8868076030983));
#71016=CARTESIAN_POINT('Ctrl Pts',(-19.9942591430928,21.006608717098,28.0856945144732));
#71017=CARTESIAN_POINT('Ctrl Pts',(-19.4880894883424,25.1670455539585,28.2845814258481));
#71018=CARTESIAN_POINT('Ctrl Pts',(-22.7146929737878,27.8417193740874,28.483468337223));
#71019=CARTESIAN_POINT('Ctrl Pts',(-26.7091242637221,26.5730261189747,28.6823552485979));
#71020=CARTESIAN_POINT('Ctrl Pts',(-27.800783601434,22.5264202402148,28.8812421599727));
#71021=CARTESIAN_POINT('Ctrl Pts',(-24.9866344909904,19.4210825872784,29.0801290713476));
#71022=CARTESIAN_POINT('Ctrl Pts',(-20.8524414419848,20.1092462471125,29.2790159827225));
#71023=CARTESIAN_POINT('Ctrl Pts',(-19.1975548654738,23.9610197697405,29.4779028940975));
#71024=CARTESIAN_POINT('Ctrl Pts',(-21.5419621600858,27.4322721963604,29.6767898054723));
#71025=CARTESIAN_POINT('Ctrl Pts',(-25.7326999905548,27.3421218489336,29.8756767168472));
#71026=CARTESIAN_POINT('Ctrl Pts',(-27.9167437462655,23.7552312243062,30.074606513978));
#71027=CARTESIAN_POINT('Ctrl Pts',(-26.6988816812223,21.2548018888855,30.207240673984));
#71028=CARTESIAN_POINT('Ctrl Pts',(-25.6949495301469,20.5396876139378,30.2735791968649));
#71029=CARTESIAN_POINT('Ctrl Pts',(-25.3002789331219,27.0757977803642,-74.998270464385));
#71030=CARTESIAN_POINT('Ctrl Pts',(-26.4751253509978,26.4926221000403,-74.93197482726));
#71031=CARTESIAN_POINT('Ctrl Pts',(-28.1754011787373,24.0694996479516,-74.79938355301));
#71032=CARTESIAN_POINT('Ctrl Pts',(-26.4837483309012,19.9311312672286,-74.6004966416352));
#71033=CARTESIAN_POINT('Ctrl Pts',(-22.0927467074531,19.1303002597153,-74.4016097302603));
#71034=CARTESIAN_POINT('Ctrl Pts',(-19.0429812726389,22.3850346168187,-74.2027228188854));
#71035=CARTESIAN_POINT('Ctrl Pts',(-20.1340100833004,26.7136450865977,-74.0038359075104));
#71036=CARTESIAN_POINT('Ctrl Pts',(-24.3648079623233,28.1337076326876,-73.8049489961356));
#71037=CARTESIAN_POINT('Ctrl Pts',(-27.8468168625814,25.3428413000204,-73.6060620847608));
#71038=CARTESIAN_POINT('Ctrl Pts',(-27.3807965561229,20.9042730835607,-73.407175173386));
#71039=CARTESIAN_POINT('Ctrl Pts',(-23.3947520922001,18.8973817856161,-73.2082882620109));
#71040=CARTESIAN_POINT('Ctrl Pts',(-19.5516411735125,21.1659538450954,-73.0094013506361));
#71041=CARTESIAN_POINT('Ctrl Pts',(-19.3828929156757,25.6255632813351,-72.8105144392611));
#71042=CARTESIAN_POINT('Ctrl Pts',(-23.0436065423778,28.1781015326929,-72.6116275278863));
#71043=CARTESIAN_POINT('Ctrl Pts',(-27.1698786638517,26.4780582930873,-72.4127406165114));
#71044=CARTESIAN_POINT('Ctrl Pts',(-27.9700245539433,22.0875995404682,-72.2138537051365));
#71045=CARTESIAN_POINT('Ctrl Pts',(-24.7087729478585,19.0412003055027,-72.0149667937617));
#71046=CARTESIAN_POINT('Ctrl Pts',(-20.3829402285396,20.1382348854171,-71.8160798823866));
#71047=CARTESIAN_POINT('Ctrl Pts',(-18.9675984832563,24.3706259142265,-71.6171929710119));
#71048=CARTESIAN_POINT('Ctrl Pts',(-21.7633275223502,27.8491625539056,-71.4183060596369));
#71049=CARTESIAN_POINT('Ctrl Pts',(-26.2010890016861,27.3773657979069,-71.219419148262));
#71050=CARTESIAN_POINT('Ctrl Pts',(-28.2029565915712,23.3887762096687,-71.0205322368872));
#71051=CARTESIAN_POINT('Ctrl Pts',(-25.9293835962292,19.5485697902788,-70.8216453255123));
#71052=CARTESIAN_POINT('Ctrl Pts',(-21.4695908899928,19.3855704600358,-70.6227584141375));
#71053=CARTESIAN_POINT('Ctrl Pts',(-18.9217498106796,23.0495608804504,-70.4238715027624));
#71054=CARTESIAN_POINT('Ctrl Pts',(-20.6271103053749,27.173644458905,-70.2249845913878));
#71055=CARTESIAN_POINT('Ctrl Pts',(-25.0185906614429,27.9681380786542,-70.0260976800127));
#71056=CARTESIAN_POINT('Ctrl Pts',(-28.0607927724171,24.7029694506781,-69.8272107686379));
#71057=CARTESIAN_POINT('Ctrl Pts',(-26.958190832065,20.3785517110777,-69.6283238572629));
#71058=CARTESIAN_POINT('Ctrl Pts',(-22.7239825396399,18.9686581083402,-69.4294369458881));
#71059=CARTESIAN_POINT('Ctrl Pts',(-19.2490463135321,21.7688613262589,-69.2305500345131));
#71060=CARTESIAN_POINT('Ctrl Pts',(-19.726553919893,26.2060120245128,-69.0316631231383));
#71061=CARTESIAN_POINT('Ctrl Pts',(-23.7177163542527,28.2027449203469,-68.8327762117633));
#71062=CARTESIAN_POINT('Ctrl Pts',(-27.554993734307,25.9242317772028,-68.6338893003885));
#71063=CARTESIAN_POINT('Ctrl Pts',(-27.7122534952017,21.464232987742,-68.4350023890136));
#71064=CARTESIAN_POINT('Ctrl Pts',(-24.0449872501318,18.9211092938514,-68.2361154776388));
#71065=CARTESIAN_POINT('Ctrl Pts',(-19.9231017453993,20.6317757489323,-68.0372285662638));
#71066=CARTESIAN_POINT('Ctrl Pts',(-19.1342602816024,25.0242749213373,-67.8383416548889));
#71067=CARTESIAN_POINT('Ctrl Pts',(-22.4033412812393,28.0622724941539,-67.6394547435142));
#71068=CARTESIAN_POINT('Ctrl Pts',(-26.7263364780072,26.9541062776738,-67.4405678321392));
#71069=CARTESIAN_POINT('Ctrl Pts',(-28.1307798156237,22.7180870678451,-67.2416809207643));
#71070=CARTESIAN_POINT('Ctrl Pts',(-25.3261069439786,19.2467573632969,-67.0427940093892));
#71071=CARTESIAN_POINT('Ctrl Pts',(-20.8895744350682,19.7299748422869,-66.8439070980146));
#71072=CARTESIAN_POINT('Ctrl Pts',(-18.8979795086559,23.7237036117087,-66.6450201866394));
#71073=CARTESIAN_POINT('Ctrl Pts',(-21.1814290427109,27.5580455448236,-66.4461332752648));
#71074=CARTESIAN_POINT('Ctrl Pts',(-25.6416265200303,27.7095655036835,-66.2472463638896));
#71075=CARTESIAN_POINT('Ctrl Pts',(-28.1800286213416,24.0390294928702,-66.0483594525151));
#71076=CARTESIAN_POINT('Ctrl Pts',(-26.4640590365463,19.9193488961884,-65.84947254114));
#71077=CARTESIAN_POINT('Ctrl Pts',(-22.070548323843,19.1361608906749,-65.6505856297653));
#71078=CARTESIAN_POINT('Ctrl Pts',(-19.0367603199271,22.4091488500043,-65.4516987183902));
#71079=CARTESIAN_POINT('Ctrl Pts',(-20.1504889775927,26.7307143431692,-65.2528118070154));
#71080=CARTESIAN_POINT('Ctrl Pts',(-24.3883120890633,28.1297050902813,-65.0539248956404));
#71081=CARTESIAN_POINT('Ctrl Pts',(-27.8560295230445,25.3205672095992,-64.8550379842656));
#71082=CARTESIAN_POINT('Ctrl Pts',(-27.3671029716606,20.8846602378549,-64.6561510728907));
#71083=CARTESIAN_POINT('Ctrl Pts',(-23.3708144814982,18.8982065791922,-64.4572641615158));
#71084=CARTESIAN_POINT('Ctrl Pts',(-19.5394143456281,21.1865887224265,-64.2583772501409));
#71085=CARTESIAN_POINT('Ctrl Pts',(-19.3936344397536,25.6469775007352,-64.059490338766));
#71086=CARTESIAN_POINT('Ctrl Pts',(-23.0674341372756,28.1806538054564,-63.8606034273911));
#71087=CARTESIAN_POINT('Ctrl Pts',(-27.1849030030193,26.4593839328764,-63.6617165160162));
#71088=CARTESIAN_POINT('Ctrl Pts',(-27.9624362531557,22.0648689562775,-63.4628296046415));
#71089=CARTESIAN_POINT('Ctrl Pts',(-24.685546754758,19.0352955457279,-63.2639426932664));
#71090=CARTESIAN_POINT('Ctrl Pts',(-20.365418122441,20.1545848000565,-63.0650557818915));
#71091=CARTESIAN_POINT('Ctrl Pts',(-18.9718822827999,24.3942047946143,-62.8661688705168));
#71092=CARTESIAN_POINT('Ctrl Pts',(-21.7854805201097,27.8583042149004,-62.6672819591418));
#71093=CARTESIAN_POINT('Ctrl Pts',(-26.2207546080739,27.363669400868,-62.468395047767));
#71094=CARTESIAN_POINT('Ctrl Pts',(-28.2020637090825,23.3648278084966,-62.2695081363919));
#71095=CARTESIAN_POINT('Ctrl Pts',(-25.908752746618,19.5363758153198,-62.0706212250171));
#71096=CARTESIAN_POINT('Ctrl Pts',(-21.4481800544803,19.3963362038671,-61.8717343136422));
#71097=CARTESIAN_POINT('Ctrl Pts',(-18.9192337425472,23.0733935036625,-61.6728474022673));
#71098=CARTESIAN_POINT('Ctrl Pts',(-20.6458010521971,27.1886438192408,-61.4739604908924));
#71099=CARTESIAN_POINT('Ctrl Pts',(-25.0413130146292,27.9605210262733,-61.2750735795176));
#71100=CARTESIAN_POINT('Ctrl Pts',(-28.066666814325,24.6797354158921,-61.0761866681428));
#71101=CARTESIAN_POINT('Ctrl Pts',(-26.9418188170664,20.3610507992892,-60.8772997567678));
#71102=CARTESIAN_POINT('Ctrl Pts',(-22.7004089609511,18.9729721750507,-60.6784128453929));
#71103=CARTESIAN_POINT('Ctrl Pts',(-19.2399332914964,21.7910261091923,-60.4795259340178));
#71104=CARTESIAN_POINT('Ctrl Pts',(-19.7402755489783,26.2256599678099,-60.2806390226432));
#71105=CARTESIAN_POINT('Ctrl Pts',(-23.7416636207986,28.2018212297804,-60.0817521112681));
#71106=CARTESIAN_POINT('Ctrl Pts',(-27.567161130716,25.9035852461977,-59.8828651998933));
#71107=CARTESIAN_POINT('Ctrl Pts',(-27.7014602158176,21.4428360276963,-59.6839782885185));
#71108=CARTESIAN_POINT('Ctrl Pts',(-24.0211514035796,18.9186238969152,-59.4850913771435));
#71109=CARTESIAN_POINT('Ctrl Pts',(-19.9081264537191,20.6504857841465,-59.2862044657685));
#71110=CARTESIAN_POINT('Ctrl Pts',(-19.1419065681502,25.0469874526984,-59.0873175543938));
#71111=CARTESIAN_POINT('Ctrl Pts',(-22.4265828569774,28.0681166310412,-58.8884306430189));
#71112=CARTESIAN_POINT('Ctrl Pts',(-26.743816305392,26.9377117537917,-58.6895437316441));
#71113=CARTESIAN_POINT('Ctrl Pts',(-28.1264354153342,22.6945190606133,-58.490656820269));
#71114=CARTESIAN_POINT('Ctrl Pts',(-25.3039304515362,19.2376728731248,-58.2917699088942));
#71115=CARTESIAN_POINT('Ctrl Pts',(-20.8699441667711,19.7437217454045,-58.0928829975193));
#71116=CARTESIAN_POINT('Ctrl Pts',(-18.8989340166969,23.7476496696962,-57.8939960861445));
#71117=CARTESIAN_POINT('Ctrl Pts',(-21.2020912151292,27.5701863606814,-57.6951091747695));
#71118=CARTESIAN_POINT('Ctrl Pts',(-25.6630095722369,27.6987446970098,-57.4962222633946));
#71119=CARTESIAN_POINT('Ctrl Pts',(-28.1824833413424,24.0151904675449,-57.2973353520197));
#71120=CARTESIAN_POINT('Ctrl Pts',(-26.4453297447866,19.9043976952695,-57.0984484406449));
#71121=CARTESIAN_POINT('Ctrl Pts',(-22.0478456514677,19.1438364001541,-56.89956152927));
#71122=CARTESIAN_POINT('Ctrl Pts',(-19.0309460979801,22.4323979274461,-56.700674617895));
#71123=CARTESIAN_POINT('Ctrl Pts',(-20.1669059830785,26.7481730576014,-56.5017877065202));
#71124=CARTESIAN_POINT('Ctrl Pts',(-24.4118744858731,28.1253303633956,-56.3029007951453));
#71125=CARTESIAN_POINT('Ctrl Pts',(-27.8650854662716,25.2983790444879,-56.1040138837703));
#71126=CARTESIAN_POINT('Ctrl Pts',(-27.353330817297,20.8650476770091,-55.9051269723955));
#71127=CARTESIAN_POINT('Ctrl Pts',(-23.3468696717177,18.8991919031584,-55.7062400610207));
#71128=CARTESIAN_POINT('Ctrl Pts',(-19.5273001304339,21.2072665020213,-55.5073531496458));
#71129=CARTESIAN_POINT('Ctrl Pts',(-19.4044827557931,25.6683466096977,-55.308466238271));
#71130=CARTESIAN_POINT('Ctrl Pts',(-23.0912763018941,28.1830778444516,-55.1095793268959));
#71131=CARTESIAN_POINT('Ctrl Pts',(-27.1998300884145,26.4406354155924,-54.910692415521));
#71132=CARTESIAN_POINT('Ctrl Pts',(-27.9547315334577,22.0421761804862,-54.7118055041462));
#71133=CARTESIAN_POINT('Ctrl Pts',(-24.6622902141166,19.0295112483513,-54.5129185927712));
#71134=CARTESIAN_POINT('Ctrl Pts',(-20.3479805498764,20.1710242599562,-54.3140316813965));
#71135=CARTESIAN_POINT('Ctrl Pts',(-18.9762873290365,24.4177615419788,-54.1151447700214));
#71136=CARTESIAN_POINT('Ctrl Pts',(-21.8076803211424,27.8673315961845,-53.9162578586467));
#71137=CARTESIAN_POINT('Ctrl Pts',(-26.2403494289864,27.3498720180674,-53.7173709472717));
#71138=CARTESIAN_POINT('Ctrl Pts',(-28.201047570823,23.3408842865797,-53.5184840358969));
#71139=CARTESIAN_POINT('Ctrl Pts',(-25.8880593940927,19.5242882208526,-53.3195971245218));
#71140=CARTESIAN_POINT('Ctrl Pts',(-21.4268249241531,19.4072120113058,-53.1207102131472));
#71141=CARTESIAN_POINT('Ctrl Pts',(-18.9168403885721,23.0972387680874,-52.9218233017722));
#71142=CARTESIAN_POINT('Ctrl Pts',(-20.6645687639545,27.2035467643904,-52.7229363903972));
#71143=CARTESIAN_POINT('Ctrl Pts',(-25.0639958562534,27.9527871091166,-52.5240494790225));
#71144=CARTESIAN_POINT('Ctrl Pts',(-28.0724211775514,24.656471450568,-52.3251625676475));
#71145=CARTESIAN_POINT('Ctrl Pts',(-26.9253569299792,20.3436343974716,-52.1262756562727));
#71146=CARTESIAN_POINT('Ctrl Pts',(-22.6768579020457,18.9774075333426,-51.9273887448976));
#71147=CARTESIAN_POINT('Ctrl Pts',(-19.2309344871063,21.8132375093799,-51.7285018335229));
#71148=CARTESIAN_POINT('Ctrl Pts',(-19.7540981373651,26.2452370163368,-51.5296149221478));
#71149=CARTESIAN_POINT('Ctrl Pts',(-23.7656058151973,28.2007742789105,-51.3307280107731));
#71150=CARTESIAN_POINT('Ctrl Pts',(-27.5792220844372,25.8828763550135,-51.1318410993982));
#71151=CARTESIAN_POINT('Ctrl Pts',(-27.690556934992,21.4214949113717,-50.9329541880232));
#71152=CARTESIAN_POINT('Ctrl Pts',(-23.99730307884,18.9162612319241,-50.7340672766484));
#71153=CARTESIAN_POINT('Ctrl Pts',(-19.8932476734969,20.669272659295,-50.5351803652735));
#71154=CARTESIAN_POINT('Ctrl Pts',(-19.1496696699568,25.0696603225891,-50.3362934538984));
#71155=CARTESIAN_POINT('Ctrl Pts',(-22.4498542084553,28.0738410505872,-50.1374065425237));
#71156=CARTESIAN_POINT('Ctrl Pts',(-26.761211507618,26.9212274667807,-49.9385196311488));
#71157=CARTESIAN_POINT('Ctrl Pts',(-28.1219697523327,22.6709737291715,-49.739632719774));
#71158=CARTESIAN_POINT('Ctrl Pts',(-25.2817074889795,19.2287026605322,-49.5407458083989));
#71159=CARTESIAN_POINT('Ctrl Pts',(-20.8503849230525,19.757569516485,-49.3418588970242));
#71160=CARTESIAN_POINT('Ctrl Pts',(-18.9000117784432,23.7715904969243,-49.1429719856492));
#71161=CARTESIAN_POINT('Ctrl Pts',(-21.2228156106747,27.5822206536816,-48.9440850742744));
#71162=CARTESIAN_POINT('Ctrl Pts',(-25.6843366392143,27.687813960855,-48.7451981628995));
#71163=CARTESIAN_POINT('Ctrl Pts',(-28.1848153134365,23.9913391219875,-48.5463112515245));
#71164=CARTESIAN_POINT('Ctrl Pts',(-26.4265237373615,19.8895431046163,-48.3474243401496));
#71165=CARTESIAN_POINT('Ctrl Pts',(-22.0251827908608,19.1516286737538,-48.1485374287749));
#71166=CARTESIAN_POINT('Ctrl Pts',(-19.0252516315952,22.4556766265364,-47.9496505173999));
#71167=CARTESIAN_POINT('Ctrl Pts',(-20.1834126427124,26.7655470314266,-47.750763606025));
#71168=CARTESIAN_POINT('Ctrl Pts',(-24.435414050856,28.1208344030802,-47.5518766946501));
#71169=CARTESIAN_POINT('Ctrl Pts',(-27.8740270722105,25.2761445563675,-47.3529897832752));
#71170=CARTESIAN_POINT('Ctrl Pts',(-27.339457886457,20.8455062704923,-47.1541028719002));
#71171=CARTESIAN_POINT('Ctrl Pts',(-23.3229302513102,18.9003004739963,-46.9552159605255));
#71172=CARTESIAN_POINT('Ctrl Pts',(-19.5152925180855,21.2280063676051,-46.7563290491504));
#71173=CARTESIAN_POINT('Ctrl Pts',(-19.4154409291741,25.6896595920065,-46.5574421377758));
#71174=CARTESIAN_POINT('Ctrl Pts',(-23.1151306287675,28.1853791197866,-46.3585552264007));
#71175=CARTESIAN_POINT('Ctrl Pts',(-27.2146604648968,26.4218103070366,-46.159668315026));
#71176=CARTESIAN_POINT('Ctrl Pts',(-27.9469101009703,22.0195233666965,-45.9607814036509));
#71177=CARTESIAN_POINT('Ctrl Pts',(-24.6390042059674,19.0238467445585,-45.761894492276));
#71178=CARTESIAN_POINT('Ctrl Pts',(-20.3306278332266,20.1875532648752,-45.5630075809012));
#71179=CARTESIAN_POINT('Ctrl Pts',(-18.9808135792194,24.4412953015176,-45.3641206695263));
#71180=CARTESIAN_POINT('Ctrl Pts',(-21.8299262980028,27.8762445806607,-45.1652337581514));
#71181=CARTESIAN_POINT('Ctrl Pts',(-26.2598729659374,27.3359739504438,-44.9663468467766));
#71182=CARTESIAN_POINT('Ctrl Pts',(-28.1999081927296,23.3169463126407,-44.7674599354016));
#71183=CARTESIAN_POINT('Ctrl Pts',(-25.8673040928193,19.5123073090426,-44.5685730240267));
#71184=CARTESIAN_POINT('Ctrl Pts',(-21.4055260618107,19.4181976037643,-44.3696861126518));
#71185=CARTESIAN_POINT('Ctrl Pts',(-18.9145698138075,23.1210960367697,-44.1707992012769));
#71186=CARTESIAN_POINT('Ctrl Pts',(-20.6834129424635,27.2183529021403,-43.9719122899021));
#71187=CARTESIAN_POINT('Ctrl Pts',(-25.0866385857089,27.9449365306953,-43.7730253785271));
#71188=CARTESIAN_POINT('Ctrl Pts',(-28.0780557093708,24.6331781719254,-43.5741384671524));
#71189=CARTESIAN_POINT('Ctrl Pts',(-26.9088056071499,20.3263029667358,-43.3752515557773));
#71190=CARTESIAN_POINT('Ctrl Pts',(-22.6533299869271,18.9819640658969,-43.1763646444026));
#71191=CARTESIAN_POINT('Ctrl Pts',(-19.2220501388541,21.835494938137,-42.9774777330275));
#71192=CARTESIAN_POINT('Ctrl Pts',(-19.7680213187548,26.2647426513878,-42.7785908216527));
#71193=CARTESIAN_POINT('Ctrl Pts',(-23.7895423030223,28.1996040954486,-42.5797039102778));
#71194=CARTESIAN_POINT('Ctrl Pts',(-27.5911762758664,25.862105652425,-42.3808169989029));
#71195=CARTESIAN_POINT('Ctrl Pts',(-27.6795439416498,21.4002102042704,-42.1819300875281));
#71196=CARTESIAN_POINT('Ctrl Pts',(-23.9734429078603,18.9140213614905,-41.9830431761531));
#71197=CARTESIAN_POINT('Ctrl Pts',(-19.8784657990009,20.6881358765479,-41.7841562647783));
#71198=CARTESIAN_POINT('Ctrl Pts',(-19.1575493813103,25.0922929302101,-41.5852693534033));
#71199=CARTESIAN_POINT('Ctrl Pts',(-22.4731547190136,28.0794456011015,-41.3863824420285));
#71200=CARTESIAN_POINT('Ctrl Pts',(-26.7785216237357,26.904653853453,-41.1874955306535));
#71201=CARTESIAN_POINT('Ctrl Pts',(-28.1173829449534,22.6474516974395,-40.9886086192788));
#71202=CARTESIAN_POINT('Ctrl Pts',(-25.2594386451877,19.219846963218,-40.7897217079038));
#71203=CARTESIAN_POINT('Ctrl Pts',(-20.8308972222064,19.7715177885814,-40.5908347965289));
#71204=CARTESIAN_POINT('Ctrl Pts',(-18.9012127653357,23.7955254589928,-40.3919478851541));
#71205=CARTESIAN_POINT('Ctrl Pts',(-21.2436016801787,27.5941481049319,-40.1930609737791));
#71206=CARTESIAN_POINT('Ctrl Pts',(-25.7056071558235,27.6767735848687,-39.9941740624042));
#71207=CARTESIAN_POINT('Ctrl Pts',(-28.1870244758296,23.9674760882269,-39.7952871510293));
#71208=CARTESIAN_POINT('Ctrl Pts',(-26.4076415126053,19.8747855178556,-39.5964002396544));
#71209=CARTESIAN_POINT('Ctrl Pts',(-22.0025603425576,19.1595375049891,-39.3975133282797));
#71210=CARTESIAN_POINT('Ctrl Pts',(-19.0196770716683,22.4789843304208,-39.1986264169047));
#71211=CARTESIAN_POINT('Ctrl Pts',(-20.2000085190899,26.7828358042576,-38.9997395055298));
#71212=CARTESIAN_POINT('Ctrl Pts',(-24.4589301602452,28.1162173284725,-38.800852594155));
#71213=CARTESIAN_POINT('Ctrl Pts',(-27.8828541039201,25.253864334422,-38.6019656827801));
#71214=CARTESIAN_POINT('Ctrl Pts',(-27.3254845467546,20.8260365361259,-38.4030787714051));
#71215=CARTESIAN_POINT('Ctrl Pts',(-23.2989968546387,18.9015322623302,-38.2041918600302));
#71216=CARTESIAN_POINT('Ctrl Pts',(-19.5033918267683,21.2488077695991,-38.0053049486554));
#71217=CARTESIAN_POINT('Ctrl Pts',(-19.4265086695198,25.7109158828961,-37.8064180372804));
#71218=CARTESIAN_POINT('Ctrl Pts',(-23.1389964857879,28.1875575704805,-37.6075311259056));
#71219=CARTESIAN_POINT('Ctrl Pts',(-27.2293937394812,26.4029091060492,-37.4086442145307));
#71220=CARTESIAN_POINT('Ctrl Pts',(-27.9389721629514,21.9969111151776,-37.2097573031558));
#71221=CARTESIAN_POINT('Ctrl Pts',(-24.6156893473584,19.0183021844513,-37.010870391781));
#71222=CARTESIAN_POINT('Ctrl Pts',(-20.3133604323151,20.2041713768168,-36.811983480406));
#71223=CARTESIAN_POINT('Ctrl Pts',(-18.9854609134091,24.4648054496174,-36.6130965690311));
#71224=CARTESIAN_POINT('Ctrl Pts',(-21.8522178612022,27.8850429321467,-36.4142096576563));
#71225=CARTESIAN_POINT('Ctrl Pts',(-26.2793247015791,27.3219755662776,-36.2153227462814));
#71226=CARTESIAN_POINT('Ctrl Pts',(-28.1986456049942,23.2930145210038,-36.0164358349064));
#71227=CARTESIAN_POINT('Ctrl Pts',(-25.8464873927859,19.5004333973679,-35.8175489235315));
#71228=CARTESIAN_POINT('Ctrl Pts',(-21.3842840318447,19.4292926901393,-35.6186620121567));
#71229=CARTESIAN_POINT('Ctrl Pts',(-18.9124220784208,23.1449646775239,-35.4197751007818));
#71230=CARTESIAN_POINT('Ctrl Pts',(-20.7023330883783,27.2330618401476,-35.2208881894068));
#71231=CARTESIAN_POINT('Ctrl Pts',(-25.1092406029936,27.9369694990394,-35.0220012780321));
#71232=CARTESIAN_POINT('Ctrl Pts',(-28.0835702604755,24.609856197205,-34.8231143666572));
#71233=CARTESIAN_POINT('Ctrl Pts',(-26.8921652871665,20.3090569663418,-34.6242274552823));
#71234=CARTESIAN_POINT('Ctrl Pts',(-22.6298258390536,18.9866416519715,-34.4253405439073));
#71235=CARTESIAN_POINT('Ctrl Pts',(-19.2132804821634,21.8577978056717,-34.2264536325324));
#71236=CARTESIAN_POINT('Ctrl Pts',(-19.782044724201,26.2841763560894,-34.0275667211576));
#71237=CARTESIAN_POINT('Ctrl Pts',(-23.8134724499895,28.1983107104028,-33.8286798097826));
#71238=CARTESIAN_POINT('Ctrl Pts',(-27.6030233882333,25.841273688828,-33.6297928984078));
#71239=CARTESIAN_POINT('Ctrl Pts',(-27.6684215276209,21.3789824704085,-33.4309059870329));
#71240=CARTESIAN_POINT('Ctrl Pts',(-23.9495715229028,18.9119043449678,-33.232019075658));
#71241=CARTESIAN_POINT('Ctrl Pts',(-19.8637812219313,20.7070749360553,-33.0331321642831));
#71242=CARTESIAN_POINT('Ctrl Pts',(-19.1655454934085,25.1148846758278,-32.8342452529083));
#71243=CARTESIAN_POINT('Ctrl Pts',(-22.49648377122,28.0849301340709,-32.6353583415332));
#71244=CARTESIAN_POINT('Ctrl Pts',(-26.79574619505,26.887991352987,-32.4364714301584));
#71245=CARTESIAN_POINT('Ctrl Pts',(-28.1126751147405,22.6239535887192,-32.2375845187835));
#71246=CARTESIAN_POINT('Ctrl Pts',(-25.2371245102552,19.2111060158465,-32.0386976074086));
#71247=CARTESIAN_POINT('Ctrl Pts',(-20.8114815806304,19.7855661920827,-31.8398106960337));
#71248=CARTESIAN_POINT('Ctrl Pts',(-18.9025369455497,23.8194539216577,-31.6409237846589));
#71249=CARTESIAN_POINT('Ctrl Pts',(-21.2644488728379,27.6059683983702,-31.4420368732841));
#71250=CARTESIAN_POINT('Ctrl Pts',(-25.7268205584246,27.6656238616063,-31.243149961909));
#71251=CARTESIAN_POINT('Ctrl Pts',(-28.1891107699821,23.9436019986013,-31.0442630505341));
#71252=CARTESIAN_POINT('Ctrl Pts',(-26.3886835708716,19.8601253260437,-30.8453761391593));
#71253=CARTESIAN_POINT('Ctrl Pts',(-21.9799789060225,19.1675626842868,-30.6464892277844));
#71254=CARTESIAN_POINT('Ctrl Pts',(-19.0142225659176,22.5023204214765,-30.4476023164095));
#71255=CARTESIAN_POINT('Ctrl Pts',(-20.2166931724425,26.8000389179654,-30.2487154050346));
#71256=CARTESIAN_POINT('Ctrl Pts',(-24.4824221908955,28.1114792619185,-30.0498284936597));
#71257=CARTESIAN_POINT('Ctrl Pts',(-27.891566327496,25.2315389690475,-29.8509415822849));
#71258=CARTESIAN_POINT('Ctrl Pts',(-27.3114111684648,20.8066389898312,-29.6520546709101));
#71259=CARTESIAN_POINT('Ctrl Pts',(-23.2750701159057,18.9028872355194,-29.453167759535));
#71260=CARTESIAN_POINT('Ctrl Pts',(-19.4915983718348,21.2696701567942,-29.2542808481603));
#71261=CARTESIAN_POINT('Ctrl Pts',(-19.4376856835497,25.7321149191034,-29.0553939367852));
#71262=CARTESIAN_POINT('Ctrl Pts',(-23.162873240542,28.1896131388074,-28.8565070254105));
#71263=CARTESIAN_POINT('Ctrl Pts',(-27.2440295217556,26.3839323134868,-28.6576201140354));
#71264=CARTESIAN_POINT('Ctrl Pts',(-27.9309179297455,21.9743400251241,-28.4587332026606));
#71265=CARTESIAN_POINT('Ctrl Pts',(-24.5923462561019,19.0128777149528,-28.2598462912857));
#71266=CARTESIAN_POINT('Ctrl Pts',(-20.296178804705,20.2208781554236,-28.0609593799109));
#71267=CARTESIAN_POINT('Ctrl Pts',(-18.9902292084572,24.4882913632907,-27.862072468536));
#71268=CARTESIAN_POINT('Ctrl Pts',(-21.8745544200441,27.893726417498,-27.663185557161));
#71269=CARTESIAN_POINT('Ctrl Pts',(-26.2987041204669,27.3078772365071,-27.4642986457862));
#71270=CARTESIAN_POINT('Ctrl Pts',(-28.1972598410737,23.2690895458294,-27.2654117344113));
#71271=CARTESIAN_POINT('Ctrl Pts',(-25.8256098456067,19.4886668004713,-27.0665248230364));
#71272=CARTESIAN_POINT('Ctrl Pts',(-21.3630993971404,19.4404969764257,-26.8676379116614));
#71273=CARTESIAN_POINT('Ctrl Pts',(-18.9103972393238,23.1688440578629,-26.6687510002866));
#71274=CARTESIAN_POINT('Ctrl Pts',(-20.7213287003407,27.2476731886452,-26.4698640889118));
#71275=CARTESIAN_POINT('Ctrl Pts',(-25.1318013091842,27.9288862252643,-26.2709771775369));
#71276=CARTESIAN_POINT('Ctrl Pts',(-28.0889646847377,24.5865061444081,-26.072090266162));
#71277=CARTESIAN_POINT('Ctrl Pts',(-26.875436410975,20.2918968532854,-25.8732033547871));
#71278=CARTESIAN_POINT('Ctrl Pts',(-22.6063460812538,18.9914401676168,-25.6743164434122));
#71279=CARTESIAN_POINT('Ctrl Pts',(-19.2046257494179,21.8801455209876,-25.4754295320374));
#71280=CARTESIAN_POINT('Ctrl Pts',(-19.7961679821028,26.3035376154745,-25.2765426206624));
#71281=CARTESIAN_POINT('Ctrl Pts',(-23.8373956219815,28.1968941580462,-25.0776557092874));
#71282=CARTESIAN_POINT('Ctrl Pts',(-27.6147631076054,25.8203810162416,-24.8787687979125));
#71283=CARTESIAN_POINT('Ctrl Pts',(-27.6571899876342,21.3578122722926,-24.6798818865377));
#71284=CARTESIAN_POINT('Ctrl Pts',(-23.9256895565276,18.9099102384541,-24.4809949751627));
#71285=CARTESIAN_POINT('Ctrl Pts',(-19.8491943314094,20.7260893359576,-24.2821080637879));
#71286=CARTESIAN_POINT('Ctrl Pts',(-19.1736577943654,25.137434960791,-24.083221152413));
#71287=CARTESIAN_POINT('Ctrl Pts',(-22.5198407468858,28.0902945041627,-23.8843342410382));
#71288=CARTESIAN_POINT('Ctrl Pts',(-26.8128847651328,26.8712404069166,-23.6854473296632));
#71289=CARTESIAN_POINT('Ctrl Pts',(-28.1078463864453,22.6004800256793,-23.4865604182883));
#71290=CARTESIAN_POINT('Ctrl Pts',(-25.2147656754767,19.2024800500406,-23.2876735069134));
#71291=CARTESIAN_POINT('Ctrl Pts',(-20.7921385128133,19.7997143547253,-23.0887865955386));
#71292=CARTESIAN_POINT('Ctrl Pts',(-18.9039842839965,23.8433752508465,-22.8898996841638));
#71293=CARTESIAN_POINT('Ctrl Pts',(-21.2853566362298,27.6176812207748,-22.6910127727887));
#71294=CARTESIAN_POINT('Ctrl Pts',(-25.7479762848906,27.6543650865207,-22.4921258614139));
#71295=CARTESIAN_POINT('Ctrl Pts',(-28.1910741406097,23.9197174857423,-22.2932389500389));
#71296=CARTESIAN_POINT('Ctrl Pts',(-26.3696504145205,19.8455629176561,-22.0943520386642));
#71297=CARTESIAN_POINT('Ctrl Pts',(-21.9574390796337,19.17570399899,-21.8954651272892));
#71298=CARTESIAN_POINT('Ctrl Pts',(-19.0088882588803,22.5256842813281,-21.6965782159143));
#71299=CARTESIAN_POINT('Ctrl Pts',(-20.2334661606494,26.8171559166903,-21.4976913045395));
#71300=CARTESIAN_POINT('Ctrl Pts',(-24.5058895202992,28.1066203289707,-21.2988043931646));
#71301=CARTESIAN_POINT('Ctrl Pts',(-27.9001635120761,25.2091690518364,-21.0999174817896));
#71302=CARTESIAN_POINT('Ctrl Pts',(-27.2972381245131,20.7873141456176,-20.9010305704148));
#71303=CARTESIAN_POINT('Ctrl Pts',(-23.2511506691379,18.9043653576591,-20.7021436590399));
#71304=CARTESIAN_POINT('Ctrl Pts',(-19.4799124657959,21.2905929763648,-20.5032567476651));
#71305=CARTESIAN_POINT('Ctrl Pts',(-19.448971675088,25.7532561388822,-20.30436983629));
#71306=CARTESIAN_POINT('Ctrl Pts',(-23.1867602603281,28.1915457702975,-20.1054829249152));
#71307=CARTESIAN_POINT('Ctrl Pts',(-27.2585674238914,26.364880432209,-19.9065960135404));
#71308=CARTESIAN_POINT('Ctrl Pts',(-27.9227476147789,21.9518106946394,-19.7077091021655));
#71309=CARTESIAN_POINT('Ctrl Pts',(-24.568975550759,19.0075734798047,-19.5088221907905));
#71310=CARTESIAN_POINT('Ctrl Pts',(-20.2790834056867,20.2376731579881,-19.3099352794157));
#71311=CARTESIAN_POINT('Ctrl Pts',(-18.9951183380106,24.5117524201925,-19.1110483680408));
#71312=CARTESIAN_POINT('Ctrl Pts',(-21.8969353826393,27.902294806614,-18.9121614566658));
#71313=CARTESIAN_POINT('Ctrl Pts',(-26.3180107090718,27.2936793347194,-18.713274545291));
#71314=CARTESIAN_POINT('Ctrl Pts',(-28.1957509376891,23.2451720210973,-18.5143876339161));
#71315=CARTESIAN_POINT('Ctrl Pts',(-25.804672004509,19.4770078301521,-18.3155007225413));
#71316=CARTESIAN_POINT('Ctrl Pts',(-21.3419727190624,19.451810165725,-18.1166138111664));
#71317=CARTESIAN_POINT('Ctrl Pts',(-18.9084953501721,23.192733545015,-17.9177268997915));
#71318=CARTESIAN_POINT('Ctrl Pts',(-20.7403992749922,27.2621865604517,-17.7188399884166));
#71319=CARTESIAN_POINT('Ctrl Pts',(-25.1543201064523,27.9206869235662,-17.5199530770417));
#71320=CARTESIAN_POINT('Ctrl Pts',(-28.0942388392121,24.5631286322796,-17.3210661656668));
#71321=CARTESIAN_POINT('Ctrl Pts',(-26.8586194218683,20.2748230822864,-17.1221792542919));
#71322=CARTESIAN_POINT('Ctrl Pts',(-22.5828913357095,18.9963594856784,-16.923292342917));
#71323=CARTESIAN_POINT('Ctrl Pts',(-19.1960861699567,21.9025374919005,-16.7244054315421));
#71324=CARTESIAN_POINT('Ctrl Pts',(-19.8103907182127,26.3228259164959,-16.5255185201673));
#71325=CARTESIAN_POINT('Ctrl Pts',(-23.8613111850665,28.1953544759156,-16.3266316087924));
#71326=CARTESIAN_POINT('Ctrl Pts',(-27.6263951228959,25.7994281882936,-16.1277446974175));
#71327=CARTESIAN_POINT('Ctrl Pts',(-27.6458496193105,21.3367001709045,-15.9288577860426));
#71328=CARTESIAN_POINT('Ctrl Pts',(-23.9017976415744,18.9080390947908,-15.7299708746677));
#71329=CARTESIAN_POINT('Ctrl Pts',(-19.8347055139685,20.7451785723986,-15.5310839632928));
#71330=CARTESIAN_POINT('Ctrl Pts',(-19.1818860692158,25.1599431875476,-15.3321970519179));
#71331=CARTESIAN_POINT('Ctrl Pts',(-22.5432250270827,28.0955385692284,-15.1333101405429));
#71332=CARTESIAN_POINT('Ctrl Pts',(-26.8299368798353,26.8544014591196,-14.9344232291681));
#71333=CARTESIAN_POINT('Ctrl Pts',(-28.1028968880228,22.5770316303375,-14.7355363177932));
#71334=CARTESIAN_POINT('Ctrl Pts',(-25.1923627333311,19.1939692943774,-14.5366494064184));
#71335=CARTESIAN_POINT('Ctrl Pts',(-20.7728685313203,19.8139619016018,-14.3377624950434));
#71336=CARTESIAN_POINT('Ctrl Pts',(-18.9055547423231,23.8672888126763,-14.1388755836686));
#71337=CARTESIAN_POINT('Ctrl Pts',(-21.3063244163269,27.6292862617719,-13.9399886722937));
#71338=CARTESIAN_POINT('Ctrl Pts',(-25.7690737746235,27.6429975579539,-13.7411017609188));
#71339=CARTESIAN_POINT('Ctrl Pts',(-28.1929145356861,23.8958231825571,-13.5422148495439));
#71340=CARTESIAN_POINT('Ctrl Pts',(-26.3505425479049,19.8310986785767,-13.343327938169));
#71341=CARTESIAN_POINT('Ctrl Pts',(-21.9349414606661,19.1839612333653,-13.1444410267941));
#71342=CARTESIAN_POINT('Ctrl Pts',(-19.0036742919084,22.5490752908652,-12.9455541154192));
#71343=CARTESIAN_POINT('Ctrl Pts',(-20.2503270392489,26.8341863468551,-12.7466672040443));
#71344=CARTESIAN_POINT('Ctrl Pts',(-24.5293315266039,28.1016406583841,-12.5477802926694));
#71345=CARTESIAN_POINT('Ctrl Pts',(-27.9086454298464,25.1867551755613,-12.3488933812946));
#71346=CARTESIAN_POINT('Ctrl Pts',(-27.2829657904661,20.7680625155673,-12.1500064699196));
#71347=CARTESIAN_POINT('Ctrl Pts',(-23.2272391481683,18.9059665895809,-11.9511195585448));
#71348=CARTESIAN_POINT('Ctrl Pts',(-19.4683344183123,21.3115756738845,-11.7522326471699));
#71349=CARTESIAN_POINT('Ctrl Pts',(-19.460366345071,25.7743389820187,-11.553345735795));
#71350=CARTESIAN_POINT('Ctrl Pts',(-23.2106569121722,28.1933554137386,-11.3544588244201));
#71351=CARTESIAN_POINT('Ctrl Pts',(-27.2730070606538,26.3457539670648,-11.1555719130452));
#71352=CARTESIAN_POINT('Ctrl Pts',(-27.9144614345543,21.9293237207207,-10.9566850016703));
#71353=CARTESIAN_POINT('Ctrl Pts',(-24.5455778506215,19.0023896195617,-10.7577980902953));
#71354=CARTESIAN_POINT('Ctrl Pts',(-20.262074688265,20.2545559394653,-10.5589111789205));
#71355=CARTESIAN_POINT('Ctrl Pts',(-19.0001281725137,24.5351879986362,-10.3600242675455));
#71356=CARTESIAN_POINT('Ctrl Pts',(-21.919360155923,27.9107478724438,-10.1611373561708));
#71357=CARTESIAN_POINT('Ctrl Pts',(-26.3372439557954,27.2793822371394,-9.9622504447958));
#71358=CARTESIAN_POINT('Ctrl Pts',(-28.1941189348243,23.2212625805896,-9.76336353342093));
#71359=CARTESIAN_POINT('Ctrl Pts',(-25.7836744243174,19.465456795357,-9.56447662204602));
#71360=CARTESIAN_POINT('Ctrl Pts',(-21.3209045574389,19.463231958253,-9.36558971067114));
#71361=CARTESIAN_POINT('Ctrl Pts',(-18.9067164613632,23.2166325059411,-9.16670279929625));
#71362=CARTESIAN_POINT('Ctrl Pts',(-20.7595443069883,27.2766015709828,-8.96781588792135));
#71363=CARTESIAN_POINT('Ctrl Pts',(-25.17679639808,27.9123718112153,-8.76892897654648));
#71364=CARTESIAN_POINT('Ctrl Pts',(-28.0993925841408,24.5397242802923,-8.57004206517157));
#71365=CARTESIAN_POINT('Ctrl Pts',(-26.841714765474,20.2578361057771,-8.37115515379669));
#71366=CARTESIAN_POINT('Ctrl Pts',(-22.5594622239401,19.001399475801,-8.17226824242178));
#71367=CARTESIAN_POINT('Ctrl Pts',(-19.1876619700672,21.9249731250532,-7.97338133104692));
#71368=CARTESIAN_POINT('Ctrl Pts',(-19.8247125556472,26.3420407480393,-7.774494419672));
#71369=CARTESIAN_POINT('Ctrl Pts',(-23.8852185055144,28.1936917048104,-7.57560750829713));
#71370=CARTESIAN_POINT('Ctrl Pts',(-27.637919125872,25.7784157602055,-7.37672059692223));
#71371=CARTESIAN_POINT('Ctrl Pts',(-27.6344007231541,21.3156467256866,-7.17783368554734));
#71372=CARTESIAN_POINT('Ctrl Pts',(-23.8778964111469,18.9062909635603,-6.97894677417245));
#71373=CARTESIAN_POINT('Ctrl Pts',(-19.8203151535427,20.7643421395393,-6.78005986279756));
#71374=CARTESIAN_POINT('Ctrl Pts',(-19.1902300999215,25.1824087596598,-6.58117295142267));
#71375=CARTESIAN_POINT('Ctrl Pts',(-22.5666359921586,28.1006621903073,-6.38228604004778));
#71376=CARTESIAN_POINT('Ctrl Pts',(-26.8469020872991,26.8374749558051,-6.18339912867289));
#71377=CARTESIAN_POINT('Ctrl Pts',(-28.0978267506276,22.553609024045,-5.98451221729801));
#71378=CARTESIAN_POINT('Ctrl Pts',(-25.1699162774664,19.1855739743799,-5.78562530592311));
#71379=CARTESIAN_POINT('Ctrl Pts',(-20.7536721467801,19.8283084551716,-5.58673839454821));
#71380=CARTESIAN_POINT('Ctrl Pts',(-18.9072482789147,23.8911939734695,-5.38785148317334));
#71381=CARTESIAN_POINT('Ctrl Pts',(-21.3273516575109,27.6407832138433,-5.18896457179843));
#71382=CARTESIAN_POINT('Ctrl Pts',(-25.7901124685678,27.6315215771305,-4.99007766042355));
#71383=CARTESIAN_POINT('Ctrl Pts',(-28.1946319064429,23.871919722213,-4.79119074904866));
#71384=CARTESIAN_POINT('Ctrl Pts',(-26.3313604773578,19.8167329920888,-4.59230383767377));
#71385=CARTESIAN_POINT('Ctrl Pts',(-21.9124866452764,19.1923341686068,-4.39341692629887));
#71386=CARTESIAN_POINT('Ctrl Pts',(-18.9985808031649,22.5724928302568,-4.19453001492399));
#71387=CARTESIAN_POINT('Ctrl Pts',(-20.2672753614501,26.851129757176,-3.99564310354909));
#71388=CARTESIAN_POINT('Ctrl Pts',(-24.552747588628,28.0965403821135,-3.7967561921742));
#71389=CARTESIAN_POINT('Ctrl Pts',(-27.9170118560474,25.1642979341598,-3.59786928079932));
#71390=CARTESIAN_POINT('Ctrl Pts',(-27.2685945445218,20.7488846098228,-3.39898236942442));
#71391=CARTESIAN_POINT('Ctrl Pts',(-23.2033361866205,18.9076908888542,-3.20009545804954));
#71392=CARTESIAN_POINT('Ctrl Pts',(-19.4568645361867,21.33261769334,-3.00120854667464));
#71393=CARTESIAN_POINT('Ctrl Pts',(-19.4718693915553,25.7953628898457,-2.80232163529976));
#71394=CARTESIAN_POINT('Ctrl Pts',(-23.2345625628451,28.1950420211776,-2.60343472392486));
#71395=CARTESIAN_POINT('Ctrl Pts',(-27.2873480494116,26.32655342488,-2.40454781254998));
#71396=CARTESIAN_POINT('Ctrl Pts',(-27.9060596086441,21.9068796992424,-2.20566090117508));
#71397=CARTESIAN_POINT('Ctrl Pts',(-24.5221537756973,18.9973262715892,-2.00677398980019));
#71398=CARTESIAN_POINT('Ctrl Pts',(-20.2451531031481,20.2715260524842,-1.8078870784253));
#71399=CARTESIAN_POINT('Ctrl Pts',(-19.0052585792127,24.5585974776105,-1.60900016705041));
#71400=CARTESIAN_POINT('Ctrl Pts',(-21.9418281456682,27.9190853909925,-1.41011325567552));
#71401=CARTESIAN_POINT('Ctrl Pts',(-26.3564033509824,27.2649863226212,-1.21122634430063));
#71402=CARTESIAN_POINT('Ctrl Pts',(-28.1923638757249,23.1973618578745,-1.01233943292574));
#71403=CARTESIAN_POINT('Ctrl Pts',(-25.7626176614396,19.4540140021729,-0.813452521550849));
#71404=CARTESIAN_POINT('Ctrl Pts',(-21.2998954705483,19.4747620513473,-0.614565610175962));
#71405=CARTESIAN_POINT('Ctrl Pts',(-18.9050606200354,23.2405403073507,-0.415678698801063));
#71406=CARTESIAN_POINT('Ctrl Pts',(-20.7787632890114,27.2909178382595,-0.216791787426177));
#71407=CARTESIAN_POINT('Ctrl Pts',(-25.1992295884757,27.9039411085512,-0.0179048760512818));
#71408=CARTESIAN_POINT('Ctrl Pts',(-28.1044257829564,24.5162937086299,0.180982035323599));
#71409=CARTESIAN_POINT('Ctrl Pts',(-26.8247228897429,20.2409363738893,0.379868946698492));
#71410=CARTESIAN_POINT('Ctrl Pts',(-22.5360593667856,19.0065600044316,0.578755858073388));
#71411=CARTESIAN_POINT('Ctrl Pts',(-19.1793533729794,21.9474518259315,0.777642769448271));
#71412=CARTESIAN_POINT('Ctrl Pts',(-19.8391331148967,26.3611816009374,0.976529680823165));
#71413=CARTESIAN_POINT('Ctrl Pts',(-23.9091169498129,28.1919058887919,1.17541659219806));
#71414=CARTESIAN_POINT('Ctrl Pts',(-27.649334811163,25.7573442887791,1.37430350357295));
#71415=CARTESIAN_POINT('Ctrl Pts',(-27.6228436025457,21.2946524945269,1.57319041494784));
#71416=CARTESIAN_POINT('Ctrl Pts',(-23.8539864985959,18.9046658910859,1.77207732632273));
#71417=CARTESIAN_POINT('Ctrl Pts',(-19.8060236314572,20.7835795295708,1.97096423769762));
#71418=CARTESIAN_POINT('Ctrl Pts',(-19.1986896653768,25.2048310818198,2.16985114907251));
#71419=CARTESIAN_POINT('Ctrl Pts',(-22.5900730217541,28.1056652316304,2.3687380604474));
#71420=CARTESIAN_POINT('Ctrl Pts',(-26.863779937969,26.8204613455031,2.56762497182229));
#71421=CARTESIAN_POINT('Ctrl Pts',(-28.092636108612,22.5302128274693,2.76651188319718));
#71422=CARTESIAN_POINT('Ctrl Pts',(-25.1474269026838,19.1772943125133,2.96539879457208));
#71423=CARTESIAN_POINT('Ctrl Pts',(-20.7345498678712,19.8427536352697,3.16428570594695));
#71424=CARTESIAN_POINT('Ctrl Pts',(-18.909064848895,23.9150900997717,3.36317261732185));
#71425=CARTESIAN_POINT('Ctrl Pts',(-21.3484378025882,27.6521717723351,3.56205952869672));
#71426=CARTESIAN_POINT('Ctrl Pts',(-25.8110918092263,27.6199374481484,3.76094644007167));
#71427=CARTESIAN_POINT('Ctrl Pts',(-28.1962262073723,23.8480077381194,3.95983335144652));
#71428=CARTESIAN_POINT('Ctrl Pts',(-26.3121047111783,19.8024662388638,4.15872026282142));
#71429=CARTESIAN_POINT('Ctrl Pts',(-21.8900752284872,19.2008225828429,4.3576071741963));
#71430=CARTESIAN_POINT('Ctrl Pts',(-18.9936079276205,22.5959362789698,4.55649408557119));
#71431=CARTESIAN_POINT('Ctrl Pts',(-20.2843106781455,26.8679856986754,4.75538099694606));
#71432=CARTESIAN_POINT('Ctrl Pts',(-24.5761370858766,28.0913196353095,4.95426790832101));
#71433=CARTESIAN_POINT('Ctrl Pts',(-27.9252625689805,25.1417979227188,5.15315481969587));
#71434=CARTESIAN_POINT('Ctrl Pts',(-27.2541247674984,20.7297809365728,5.35204173107077));
#71435=CARTESIAN_POINT('Ctrl Pts',(-23.1794424178906,18.9095382097875,5.55092864244564));
#71436=CARTESIAN_POINT('Ctrl Pts',(-19.4455031233554,21.3537184771459,5.74981555382054));
#71437=CARTESIAN_POINT('Ctrl Pts',(-19.4834805097256,25.8163273052579,5.9487024651954));
#71438=CARTESIAN_POINT('Ctrl Pts',(-23.2584765788788,28.1966055479217,6.14758937657036));
#71439=CARTESIAN_POINT('Ctrl Pts',(-27.301590010148,26.3072793144432,6.3464762879452));
#71440=CARTESIAN_POINT('Ctrl Pts',(-27.8975423596855,21.8844792249412,6.54536319932011));
#71441=CARTESIAN_POINT('Ctrl Pts',(-24.4987039466931,18.9923835700593,6.74425011069501));
#71442=CARTESIAN_POINT('Ctrl Pts',(-20.2283190987355,20.2885830473596,6.94313702206986));
#71443=CARTESIAN_POINT('Ctrl Pts',(-19.0105094221587,24.5819802367954,7.14202393344476));
#71444=CARTESIAN_POINT('Ctrl Pts',(-21.9643387565034,27.9273071413271,7.34091084481965));
#71445=CARTESIAN_POINT('Ctrl Pts',(-26.3754883869345,27.2504919726375,7.53979775619457));
#71446=CARTESIAN_POINT('Ctrl Pts',(-28.190485806898,23.1734704862893,7.73868466756944));
#71447=CARTESIAN_POINT('Ctrl Pts',(-25.7415022738518,19.4426797538188,7.93757157894435));
#71448=CARTESIAN_POINT('Ctrl Pts',(-21.2789460151029,19.4864001394758,8.13645849031921));
#71449=CARTESIAN_POINT('Ctrl Pts',(-18.9035278700662,23.264456315719,8.3353454016941));
#71450=CARTESIAN_POINT('Ctrl Pts',(-20.7980557117841,27.3051349829202,8.53423231306901));
#71451=CARTESIAN_POINT('Ctrl Pts',(-25.22161908319,27.8953950389761,8.73311922444391));
#71452=CARTESIAN_POINT('Ctrl Pts',(-28.109338302286,24.4928375381713,8.93200613581879));
#71453=CARTESIAN_POINT('Ctrl Pts',(-26.8076442449367,20.2241243344435,9.13089304719368));
#71454=CARTESIAN_POINT('Ctrl Pts',(-22.5126833843905,19.0118409348233,9.32977995856857));
#71455=CARTESIAN_POINT('Ctrl Pts',(-19.1711605988596,21.9699729988797,9.52866686994343));
#71456=CARTESIAN_POINT('Ctrl Pts',(-19.8536520138361,26.3802479679834,9.72755378131836));
#71457=CARTESIAN_POINT('Ctrl Pts',(-23.9330058846853,28.1899970751816,9.92644069269323));
#71458=CARTESIAN_POINT('Ctrl Pts',(-27.6606418762687,25.7362143323797,10.1253276040681));
#71459=CARTESIAN_POINT('Ctrl Pts',(-27.6111785637333,21.2737180337446,10.324214515443));
#71460=CARTESIAN_POINT('Ctrl Pts',(-23.8300685375021,18.9031639204299,10.5231014268179));
#71461=CARTESIAN_POINT('Ctrl Pts',(-19.7918313264183,20.802890232728,10.7219883381927));
#71462=CARTESIAN_POINT('Ctrl Pts',(-19.2072645414147,25.2272095598663,10.9208752495676));
#71463=CARTESIAN_POINT('Ctrl Pts',(-22.6135354948195,28.1105475606235,11.1197621609425));
#71464=CARTESIAN_POINT('Ctrl Pts',(-26.8805699846046,26.8033610790514,11.3186490723174));
#71465=CARTESIAN_POINT('Ctrl Pts',(-28.0873250995208,22.5068436605784,11.5175359836923));
#71466=CARTESIAN_POINT('Ctrl Pts',(-25.1248952049213,19.1691305281772,11.7164228950672));
#71467=CARTESIAN_POINT('Ctrl Pts',(-20.7155022013083,19.8572970591188,11.9153098064422));
#71468=CARTESIAN_POINT('Ctrl Pts',(-18.9110044041271,23.9389765583675,12.114196717817));
#71469=CARTESIAN_POINT('Ctrl Pts',(-21.3695822928042,27.6634516354658,12.3130836291919));
#71470=CARTESIAN_POINT('Ctrl Pts',(-25.8320112406749,27.6082454779718,12.5119705405668));
#71471=CARTESIAN_POINT('Ctrl Pts',(-28.1976973962274,23.8240878639119,12.7108574519416));
#71472=CARTESIAN_POINT('Ctrl Pts',(-26.2927757596185,19.7882987969516,12.9097443633166));
#71473=CARTESIAN_POINT('Ctrl Pts',(-21.867707804171,19.209426251142,13.1086312746914));
#71474=CARTESIAN_POINT('Ctrl Pts',(-18.9887557970497,22.6194050157843,13.3075181860663));
#71475=CARTESIAN_POINT('Ctrl Pts',(-20.3014325379218,26.8847537246933,13.5064050974412));
#71476=CARTESIAN_POINT('Ctrl Pts',(-24.5994993985599,28.0859785563148,13.7052920088161));
#71477=CARTESIAN_POINT('Ctrl Pts',(-27.9333973500122,25.1192557374586,13.904178920191));
#71478=CARTESIAN_POINT('Ctrl Pts',(-27.2395568428261,20.7107520020393,14.1030658315659));
#71479=CARTESIAN_POINT('Ctrl Pts',(-23.1555584751319,18.9115085034293,14.3019527429409));
#71480=CARTESIAN_POINT('Ctrl Pts',(-19.434250480881,21.3748774661597,14.5008396543157));
#71481=CARTESIAN_POINT('Ctrl Pts',(-19.4951993919029,25.8372316727265,14.6997265656906));
#71482=CARTESIAN_POINT('Ctrl Pts',(-23.2823983265842,28.1980459525395,14.8986134770655));
#71483=CARTESIAN_POINT('Ctrl Pts',(-27.31573256547,26.2879321464927,15.0975003884403));
#71484=CARTESIAN_POINT('Ctrl Pts',(-27.8889099133742,21.8621228913996,15.2963872998152));
#71485=CARTESIAN_POINT('Ctrl Pts',(-24.4752289849978,18.9875616459468,15.4952742111901));
#71486=CARTESIAN_POINT('Ctrl Pts',(-20.2115731211057,20.3057264721038,15.694161122565));
#71487=CARTESIAN_POINT('Ctrl Pts',(-19.0158805622113,24.605335656579,15.8930480339399));
#71488=CARTESIAN_POINT('Ctrl Pts',(-21.9868913919278,27.935412905582,16.0919349453148));
#71489=CARTESIAN_POINT('Ctrl Pts',(-26.3944985579235,27.2358995712689,16.2908218566897));
#71490=CARTESIAN_POINT('Ctrl Pts',(-28.1884847781097,23.1495890989232,16.4897087680645));
#71491=CARTESIAN_POINT('Ctrl Pts',(-25.7203288210831,19.431454350637,16.6885956794395));
#71492=CARTESIAN_POINT('Ctrl Pts',(-21.2580567462356,19.4981459142451,16.8874825908143));
#71493=CARTESIAN_POINT('Ctrl Pts',(-18.9021182520713,23.2883798973039,17.0863695021893));
#71494=CARTESIAN_POINT('Ctrl Pts',(-20.8174210640831,27.3192526282294,17.2852564135641));
#71495=CARTESIAN_POINT('Ctrl Pts',(-25.2439642889312,27.8867338289495,17.4841433249391));
#71496=CARTESIAN_POINT('Ctrl Pts',(-28.1141300119542,24.4693563904737,17.6830302363139));
#71497=CARTESIAN_POINT('Ctrl Pts',(-26.7904792836169,20.207400432936,17.8819171476888));
#71498=CARTESIAN_POINT('Ctrl Pts',(-22.4893348961867,19.0172421270384,18.0808040590636));
#71499=CARTESIAN_POINT('Ctrl Pts',(-19.163083864806,21.9925360471172,18.2796909704387));
#71500=CARTESIAN_POINT('Ctrl Pts',(-19.8682688677335,26.3992393439442,18.4785778818134));
#71501=CARTESIAN_POINT('Ctrl Pts',(-23.9568846771073,28.1879653145608,18.6774647931884));
#71502=CARTESIAN_POINT('Ctrl Pts',(-27.6718400215669,25.7150264509229,18.8763517045632));
#71503=CARTESIAN_POINT('Ctrl Pts',(-27.599405915825,21.2528438980745,19.0752386159382));
#71504=CARTESIAN_POINT('Ctrl Pts',(-23.8061431616591,18.9017850913926,19.274125527313));
#71505=CARTESIAN_POINT('Ctrl Pts',(-19.7777386145031,20.8222737373031,19.4730124386879));
#71506=CARTESIAN_POINT('Ctrl Pts',(-19.2159545008122,25.2495436007996,19.6718993500629));
#71507=CARTESIAN_POINT('Ctrl Pts',(-22.6370227896307,28.1153090479114,19.8707862614377));
#71508=CARTESIAN_POINT('Ctrl Pts',(-26.897271782292,26.7861746095843,20.0696731728126));
#71509=CARTESIAN_POINT('Ctrl Pts',(-28.0818938640886,22.4835021426237,20.2685600841875));
#71510=CARTESIAN_POINT('Ctrl Pts',(-25.1023217812389,19.1610828377014,20.4674469955624));
#71511=CARTESIAN_POINT('Ctrl Pts',(-20.696529651829,19.871938341337,20.6663339069373));
#71512=CARTESIAN_POINT('Ctrl Pts',(-18.9130668932155,23.9628527162975,20.8652208183122));
#71513=CARTESIAN_POINT('Ctrl Pts',(-21.3907845678583,27.6746225043341,21.0641077296871));
#71514=CARTESIAN_POINT('Ctrl Pts',(-25.8528702085764,27.5964459764219,21.2629946410619));
#71515=CARTESIAN_POINT('Ctrl Pts',(-28.1990454340238,23.8001607334355,21.4618815524368));
#71516=CARTESIAN_POINT('Ctrl Pts',(-26.2733741348695,19.7742310417702,21.6607684638117));
#71517=CARTESIAN_POINT('Ctrl Pts',(-21.8453849650347,19.2181449455185,21.8596553751866));
#71518=CARTESIAN_POINT('Ctrl Pts',(-18.9840245400275,22.6428984188101,22.0585422865615));
#71519=CARTESIAN_POINT('Ctrl Pts',(-20.3186404870729,26.9014333908998,22.2574291979364));
#71520=CARTESIAN_POINT('Ctrl Pts',(-24.6228339076079,28.0805172866607,22.4563161093113));
#71521=CARTESIAN_POINT('Ctrl Pts',(-27.9414159835821,25.0966719757166,22.6552030206861));
#71522=CARTESIAN_POINT('Ctrl Pts',(-27.2248911565355,20.6917983104636,22.8540899320611));
#71523=CARTESIAN_POINT('Ctrl Pts',(-23.1316849912363,18.9136017175688,23.0529768434359));
#71524=CARTESIAN_POINT('Ctrl Pts',(-19.4231069069434,21.3960940996979,23.2518637548108));
#71525=CARTESIAN_POINT('Ctrl Pts',(-19.5070257275519,25.858075438311,23.4507506661858));
#71526=CARTESIAN_POINT('Ctrl Pts',(-23.3063271720676,28.199363196867,23.6496375775607));
#71527=CARTESIAN_POINT('Ctrl Pts',(-27.3297753406174,26.2685124336933,23.8485244889355));
#71528=CARTESIAN_POINT('Ctrl Pts',(-27.8801624984611,21.8398112910477,24.0474114003104));
#71529=CARTESIAN_POINT('Ctrl Pts',(-24.4517295126615,18.9828606269937,24.2462983116853));
#71530=CARTESIAN_POINT('Ctrl Pts',(-20.194915614014,20.3229558725011,24.4451852230601));
#71531=CARTESIAN_POINT('Ctrl Pts',(-19.021371857025,24.628663117958,24.6440721344351));
#71532=CARTESIAN_POINT('Ctrl Pts',(-22.0094854543603,27.9434024691856,24.84295904581));
#71533=CARTESIAN_POINT('Ctrl Pts',(-26.4134333601426,27.221209504779,25.0418459571849));
#71534=CARTESIAN_POINT('Ctrl Pts',(-28.1863608425043,23.1257183293854,25.2407328685598));
#71535=CARTESIAN_POINT('Ctrl Pts',(-25.6990978639753,19.4203380886039,25.4396197799346));
#71536=CARTESIAN_POINT('Ctrl Pts',(-21.2372282179111,19.5099990672052,25.6385066913096));
#71537=CARTESIAN_POINT('Ctrl Pts',(-18.900831802597,23.3123104128807,25.8373936026844));
#71538=CARTESIAN_POINT('Ctrl Pts',(-20.836858834276,27.3332704100622,26.0362805140593));
#71539=CARTESIAN_POINT('Ctrl Pts',(-25.2662646107047,27.8779576891496,26.2351674254342));
#71540=CARTESIAN_POINT('Ctrl Pts',(-28.118800790419,24.4458509233144,26.4340543368091));
#71541=CARTESIAN_POINT('Ctrl Pts',(-26.7732284503756,20.1907650453861,26.632941248184));
#71542=CARTESIAN_POINT('Ctrl Pts',(-22.4660145402437,19.0227635647297,26.8318281595589));
#71543=CARTESIAN_POINT('Ctrl Pts',(-19.1551233482742,22.0151401333725,27.0307150709338));
#71544=CARTESIAN_POINT('Ctrl Pts',(-19.8829833583075,26.4181556775741,27.2296019823087));
#71545=CARTESIAN_POINT('Ctrl Pts',(-23.9807525639513,28.1858098072997,27.4284888936836));
#71546=CARTESIAN_POINT('Ctrl Pts',(-27.6829291964891,25.6937828173813,27.6273758050585));
#71547=CARTESIAN_POINT('Ctrl Pts',(-27.5875255059658,21.2320275977716,27.8262627164333));
#71548=CARTESIAN_POINT('Ctrl Pts',(-23.7822118827208,18.9005351860905,28.0251496278082));
#71549=CARTESIAN_POINT('Ctrl Pts',(-19.7637442119418,20.8417186808364,28.2240365391831));
#71550=CARTESIAN_POINT('Ctrl Pts',(-19.2247624424421,25.2718530975856,28.422923450558));
#71551=CARTESIAN_POINT('Ctrl Pts',(-22.6605283753441,28.1199108878517,28.6218103619329));
#71552=CARTESIAN_POINT('Ctrl Pts',(-26.9138960448389,26.7689754274264,28.8206972733079));
#71553=CARTESIAN_POINT('Ctrl Pts',(-28.0763214806764,22.4600509857223,29.0195841846826));
#71554=CARTESIAN_POINT('Ctrl Pts',(-25.0797470061916,19.1534118631149,29.2184710960576));
#71555=CARTESIAN_POINT('Ctrl Pts',(-20.6775576135736,19.8861852793049,29.4173580074325));
#71556=CARTESIAN_POINT('Ctrl Pts',(-18.9153941038522,23.9876474856138,29.6162449188074));
#71557=CARTESIAN_POINT('Ctrl Pts',(-21.4117760584397,27.6839215662933,29.8151318301822));
#71558=CARTESIAN_POINT('Ctrl Pts',(-25.8741757107666,27.5879272819239,30.0140187415572));
#71559=CARTESIAN_POINT('Ctrl Pts',(-28.1997986655813,23.7685188331541,30.212948538688));
#71560=CARTESIAN_POINT('Ctrl Pts',(-26.902989493669,21.1060008116438,30.345582698694));
#71561=CARTESIAN_POINT('Ctrl Pts',(-25.8339781016064,20.3445297244528,30.4119212215749));
#71562=CARTESIAN_POINT('Ctrl Pts',(-25.303008770126,27.07863963872,30.));
#71563=CARTESIAN_POINT('Ctrl Pts',(-25.372165991601,27.0367793117585,30.));
#71564=CARTESIAN_POINT('Ctrl Pts',(-25.4398095734417,26.9927043362926,30.));
#71565=CARTESIAN_POINT('Ctrl Pts',(-25.5058238888464,26.9464145021148,30.));
#71566=CARTESIAN_POINT('Ctrl Pts',(-25.6040445244783,26.8775413053185,30.));
#71567=CARTESIAN_POINT('Ctrl Pts',(-25.6986602703167,26.8037666196724,30.));
#71568=CARTESIAN_POINT('Ctrl Pts',(-25.7895165324835,26.7255041386418,29.9999999999999));
#71569=CARTESIAN_POINT('Ctrl Pts',(-25.8831309934207,26.6448657786811,29.9999999999999));
#71570=CARTESIAN_POINT('Ctrl Pts',(-25.9727548341034,26.5594622354632,29.9999999999999));
#71571=CARTESIAN_POINT('Ctrl Pts',(-26.0581747949051,26.4697105300558,29.9999999999999));
#71572=CARTESIAN_POINT('Ctrl Pts',(-26.1435947557068,26.3799588246483,29.9999999999999));
#71573=CARTESIAN_POINT('Ctrl Pts',(-26.2248112247842,26.2858579925564,29.9999999999999));
#71574=CARTESIAN_POINT('Ctrl Pts',(-26.3015603633575,26.1878035338793,29.9999999999999));
#71575=CARTESIAN_POINT('Ctrl Pts',(-26.3266580727016,26.1557387791535,29.9999999999999));
#71576=CARTESIAN_POINT('Ctrl Pts',(-26.351277639249,26.1232511324394,29.9999999999999));
#71577=CARTESIAN_POINT('Ctrl Pts',(-26.3754085552229,26.090354191029,29.9999999999999));
#71578=CARTESIAN_POINT('Ctrl Pts',(-26.3882478224815,26.0728508097559,29.9999999999999));
#71579=CARTESIAN_POINT('Ctrl Pts',(-26.40095096979,26.0552282690474,29.9999999999999));
#71580=CARTESIAN_POINT('Ctrl Pts',(-26.4135007908628,26.0375110010851,29.9999999999999));
#71581=CARTESIAN_POINT('Ctrl Pts',(-26.4827541683328,25.9397422250354,29.9999999999999));
#71582=CARTESIAN_POINT('Ctrl Pts',(-26.5474353352631,25.838967580728,29.9999999999999));
#71583=CARTESIAN_POINT('Ctrl Pts',(-26.6073791953875,25.7355801632597,29.9999999999999));
#71584=CARTESIAN_POINT('Ctrl Pts',(-26.6670422084197,25.632677133275,29.9999999999999));
#71585=CARTESIAN_POINT('Ctrl Pts',(-26.7220124756955,25.5271848669968,29.9999999999999));
#71586=CARTESIAN_POINT('Ctrl Pts',(-26.7720800027759,25.4194716712384,29.9999999999999));
#71587=CARTESIAN_POINT('Ctrl Pts',(-26.8217631081094,25.3125855044405,29.9999999999999));
#71588=CARTESIAN_POINT('Ctrl Pts',(-26.8666187072,25.2035115547606,29.9999999999999));
#71589=CARTESIAN_POINT('Ctrl Pts',(-26.9063912512661,25.0926034302957,29.9999999999999));
#71590=CARTESIAN_POINT('Ctrl Pts',(-26.9261217035927,25.0375838806596,29.9999999999999));
#71591=CARTESIAN_POINT('Ctrl Pts',(-26.9446004248126,24.9821129247898,29.9999999999999));
#71592=CARTESIAN_POINT('Ctrl Pts',(-26.9617912883676,24.9262340987148,29.9999999999999));
#71593=CARTESIAN_POINT('Ctrl Pts',(-26.9712190886198,24.8955890756259,29.9999999999999));
#71594=CARTESIAN_POINT('Ctrl Pts',(-26.9802594893109,24.8648213882773,29.9999999999999));
#71595=CARTESIAN_POINT('Ctrl Pts',(-26.9889060941125,24.8339383022564,29.9999999999999));
#71596=CARTESIAN_POINT('Ctrl Pts',(-26.9958124014672,24.8092710381662,29.9999999999999));
#71597=CARTESIAN_POINT('Ctrl Pts',(-27.0024674727593,24.7845301541386,29.9999999999999));
#71598=CARTESIAN_POINT('Ctrl Pts',(-27.0088679029781,24.759719389574,29.9999999999999));
#71599=CARTESIAN_POINT('Ctrl Pts',(-27.0128989714829,24.7440932694231,29.9999999999999));
#71600=CARTESIAN_POINT('Ctrl Pts',(-27.01682673476,24.7284482963229,29.9999999999999));
#71601=CARTESIAN_POINT('Ctrl Pts',(-27.0206502351512,24.7127873566539,29.9999999999999));
#71602=CARTESIAN_POINT('Ctrl Pts',(-27.0478608574413,24.6013334870476,29.9999999999999));
#71603=CARTESIAN_POINT('Ctrl Pts',(-27.0698033338671,24.489039214073,30.));
#71604=CARTESIAN_POINT('Ctrl Pts',(-27.0862843013029,24.3762416801257,30.));
#71605=CARTESIAN_POINT('Ctrl Pts',(-27.1023222682183,24.2664760899297,30.));
#71606=CARTESIAN_POINT('Ctrl Pts',(-27.1131883921371,24.1562332253948,30.));
#71607=CARTESIAN_POINT('Ctrl Pts',(-27.1186562223202,24.0458250748967,29.9999999999999));
#71608=CARTESIAN_POINT('Ctrl Pts',(-27.1239898578829,23.9381266244706,30.));
#71609=CARTESIAN_POINT('Ctrl Pts',(-27.1241869291797,23.8302703359097,30.));
#71610=CARTESIAN_POINT('Ctrl Pts',(-27.1189905917103,23.7225562298034,30.));
#71611=CARTESIAN_POINT('Ctrl Pts',(-27.1136362903252,23.6115677131976,30.));
#71612=CARTESIAN_POINT('Ctrl Pts',(-27.1025545953272,23.5007293906131,30.));
#71613=CARTESIAN_POINT('Ctrl Pts',(-27.08589991268,23.3903958165813,29.9999999999999));
#71614=CARTESIAN_POINT('Ctrl Pts',(-27.0837870586004,23.3763986275059,30.));
#71615=CARTESIAN_POINT('Ctrl Pts',(-27.0815846280796,23.3624109567061,29.9999999999999));
#71616=CARTESIAN_POINT('Ctrl Pts',(-27.079294639142,23.3484431143664,29.9999999999999));
#71617=CARTESIAN_POINT('Ctrl Pts',(-27.0612875599913,23.2386085040589,30.));
#71618=CARTESIAN_POINT('Ctrl Pts',(-27.0378465367693,23.1298348295592,30.0000000000001));
#71619=CARTESIAN_POINT('Ctrl Pts',(-27.0092238737585,23.0224446555996,30.));
#71620=CARTESIAN_POINT('Ctrl Pts',(-26.9803377976117,22.9140661744904,30.));
#71621=CARTESIAN_POINT('Ctrl Pts',(-26.9461737508747,22.807095979831,30.));
#71622=CARTESIAN_POINT('Ctrl Pts',(-26.9069416225134,22.7018862518515,30.));
#71623=CARTESIAN_POINT('Ctrl Pts',(-26.867984525552,22.5974140820921,30.));
#71624=CARTESIAN_POINT('Ctrl Pts',(-26.8240295442672,22.494677081558,30.));
#71625=CARTESIAN_POINT('Ctrl Pts',(-26.7752423137273,22.3940514357048,30.));
#71626=CARTESIAN_POINT('Ctrl Pts',(-26.7387462248728,22.3187767691279,30.));
#71627=CARTESIAN_POINT('Ctrl Pts',(-26.6995451305428,22.2446842031591,30.));
#71628=CARTESIAN_POINT('Ctrl Pts',(-26.657696641436,22.171946338547,30.));
#71629=CARTESIAN_POINT('Ctrl Pts',(-26.6486184427499,22.1561673032448,30.0000000000001));
#71630=CARTESIAN_POINT('Ctrl Pts',(-26.6394156284804,22.140452073176,30.));
#71631=CARTESIAN_POINT('Ctrl Pts',(-26.6300887346912,22.1248025043154,30.));
#71632=CARTESIAN_POINT('Ctrl Pts',(-26.6211333069317,22.1097762172616,30.));
#71633=CARTESIAN_POINT('Ctrl Pts',(-26.6120689232449,22.0948195888436,30.));
#71634=CARTESIAN_POINT('Ctrl Pts',(-26.6028964652153,22.0799340773755,30.));
#71635=CARTESIAN_POINT('Ctrl Pts',(-26.5446915134282,21.9854762478021,30.));
#71636=CARTESIAN_POINT('Ctrl Pts',(-26.4821368037367,21.8938773251799,30.));
#71637=CARTESIAN_POINT('Ctrl Pts',(-26.41541661494,21.8055000644728,30.));
#71638=CARTESIAN_POINT('Ctrl Pts',(-26.3486964261433,21.7171228037657,30.));
#71639=CARTESIAN_POINT('Ctrl Pts',(-26.2778101710931,21.6319664859985,30.));
#71640=CARTESIAN_POINT('Ctrl Pts',(-26.2029099940981,21.5504386578285,30.));
#71641=CARTESIAN_POINT('Ctrl Pts',(-26.1817683455626,21.5274262597516,30.));
#71642=CARTESIAN_POINT('Ctrl Pts',(-26.1603067285946,21.5047032650586,30.));
#71643=CARTESIAN_POINT('Ctrl Pts',(-26.138528200149,21.4822796060299,30.));
#71644=CARTESIAN_POINT('Ctrl Pts',(-26.1253039434922,21.4686636161837,30.));
#71645=CARTESIAN_POINT('Ctrl Pts',(-26.111962835437,21.4551580014475,30.));
#71646=CARTESIAN_POINT('Ctrl Pts',(-26.0985055360817,21.441765051903,30.));
#71647=CARTESIAN_POINT('Ctrl Pts',(-26.0843007187565,21.4276281588533,30.));
#71648=CARTESIAN_POINT('Ctrl Pts',(-26.0699722263908,21.4136225955588,30.));
#71649=CARTESIAN_POINT('Ctrl Pts',(-26.055525011651,21.3997543967752,30.));
#71650=CARTESIAN_POINT('Ctrl Pts',(-25.9793348914314,21.3266178267456,30.));
#71651=CARTESIAN_POINT('Ctrl Pts',(-25.8998107558415,21.2572639685655,30.));
#71652=CARTESIAN_POINT('Ctrl Pts',(-25.8170969210098,21.1920390863215,30.0000000000001));
#71653=CARTESIAN_POINT('Ctrl Pts',(-25.7366332074316,21.1285885613431,30.0000000000001));
#71654=CARTESIAN_POINT('Ctrl Pts',(-25.6531504319194,21.0690451049871,30.));
#71655=CARTESIAN_POINT('Ctrl Pts',(-25.5667624437507,21.0137725368625,30.));
#71656=CARTESIAN_POINT('Ctrl Pts',(-25.519325225581,20.9834213627177,30.));
#71657=CARTESIAN_POINT('Ctrl Pts',(-25.4710117067709,20.954358818334,30.));
#71658=CARTESIAN_POINT('Ctrl Pts',(-25.421839063434,20.9266516823442,30.));
#71659=CARTESIAN_POINT('Ctrl Pts',(-25.4258417217708,20.9227079640058,-75.));
#71660=CARTESIAN_POINT('Ctrl Pts',(-25.4842059320672,20.955216390944,-75.));
#71661=CARTESIAN_POINT('Ctrl Pts',(-25.5413694620915,20.9896046533121,-75.));
#71662=CARTESIAN_POINT('Ctrl Pts',(-25.5972316032547,21.0258485698905,-75.));
#71663=CARTESIAN_POINT('Ctrl Pts',(-25.6827790864234,21.0813526336248,-75.));
#71664=CARTESIAN_POINT('Ctrl Pts',(-25.7652758004629,21.1412057069617,-75.));
#71665=CARTESIAN_POINT('Ctrl Pts',(-25.8446406274899,21.2050026168559,-75.));
#71666=CARTESIAN_POINT('Ctrl Pts',(-25.926562532402,21.270855017495,-75.));
#71667=CARTESIAN_POINT('Ctrl Pts',(-26.0051480234115,21.3409098030885,-75.));
#71668=CARTESIAN_POINT('Ctrl Pts',(-26.0802881636455,21.4147745487126,-75.));
#71669=CARTESIAN_POINT('Ctrl Pts',(-26.1554000536204,21.4886115235847,-75.));
#71670=CARTESIAN_POINT('Ctrl Pts',(-26.2270696501425,21.5662562350316,-75.));
#71671=CARTESIAN_POINT('Ctrl Pts',(-26.2951612631559,21.6473612899045,-75.));
#71672=CARTESIAN_POINT('Ctrl Pts',(-26.3182008303572,21.6748041023069,-75.));
#71673=CARTESIAN_POINT('Ctrl Pts',(-26.3408305013503,21.7026434173748,-75.));
#71674=CARTESIAN_POINT('Ctrl Pts',(-26.3630441750331,21.7308667323941,-75.));
#71675=CARTESIAN_POINT('Ctrl Pts',(-26.3749498793541,21.7459933813391,-75.));
#71676=CARTESIAN_POINT('Ctrl Pts',(-26.3867376169378,21.7612325170237,-75.));
#71677=CARTESIAN_POINT('Ctrl Pts',(-26.3983920327574,21.7765629294232,-75.));
#71678=CARTESIAN_POINT('Ctrl Pts',(-26.4644154914187,21.8634112850157,-75.));
#71679=CARTESIAN_POINT('Ctrl Pts',(-26.5262623019746,21.9533097457026,-75.));
#71680=CARTESIAN_POINT('Ctrl Pts',(-26.5838341421057,22.0458267042707,-75.));
#71681=CARTESIAN_POINT('Ctrl Pts',(-26.6423689485129,22.13989113311,-75.));
#71682=CARTESIAN_POINT('Ctrl Pts',(-26.6964851411425,22.2366629865775,-75.));
#71683=CARTESIAN_POINT('Ctrl Pts',(-26.7460506419084,22.3357350608551,-75.));
#71684=CARTESIAN_POINT('Ctrl Pts',(-26.7960954821668,22.4357652442423,-75.));
#71685=CARTESIAN_POINT('Ctrl Pts',(-26.8415017721221,22.5381410766061,-75.));
#71686=CARTESIAN_POINT('Ctrl Pts',(-26.8820958404228,22.6424802379775,-75.));
#71687=CARTESIAN_POINT('Ctrl Pts',(-26.9024290437316,22.694742784454,-75.));
#71688=CARTESIAN_POINT('Ctrl Pts',(-26.9215542572118,22.747498419904,-75.));
#71689=CARTESIAN_POINT('Ctrl Pts',(-26.9394454329999,22.8007016269248,-75.));
#71690=CARTESIAN_POINT('Ctrl Pts',(-26.9525616993856,22.8397056277868,-75.));
#71691=CARTESIAN_POINT('Ctrl Pts',(-26.9650146663652,22.8789502128774,-75.));
#71692=CARTESIAN_POINT('Ctrl Pts',(-26.9767929984843,22.918417862835,-75.));
#71693=CARTESIAN_POINT('Ctrl Pts',(-26.980825387984,22.9319298724862,-75.));
#71694=CARTESIAN_POINT('Ctrl Pts',(-26.984778192821,22.9454664712351,-75.));
#71695=CARTESIAN_POINT('Ctrl Pts',(-26.9886485069943,22.9590178538402,-75.));
#71696=CARTESIAN_POINT('Ctrl Pts',(-27.0202317423094,23.0696022887205,-75.));
#71697=CARTESIAN_POINT('Ctrl Pts',(-27.046374962193,23.181334637174,-75.));
#71698=CARTESIAN_POINT('Ctrl Pts',(-27.0669439642748,23.293784455837,-75.));
#71699=CARTESIAN_POINT('Ctrl Pts',(-27.0874483325601,23.4058809244124,-75.));
#71700=CARTESIAN_POINT('Ctrl Pts',(-27.1024139517669,23.5186912072283,-75.));
#71701=CARTESIAN_POINT('Ctrl Pts',(-27.1116662797041,23.6318186576043,-75.));
#71702=CARTESIAN_POINT('Ctrl Pts',(-27.1202480664253,23.736747455851,-75.));
#71703=CARTESIAN_POINT('Ctrl Pts',(-27.1239145828038,23.8419499369186,-75.));
#71704=CARTESIAN_POINT('Ctrl Pts',(-27.1224887512111,23.9471230379589,-75.));
#71705=CARTESIAN_POINT('Ctrl Pts',(-27.1214315592659,24.0251043057544,-75.));
#71706=CARTESIAN_POINT('Ctrl Pts',(-27.1175740459907,24.1030697257956,-75.));
#71707=CARTESIAN_POINT('Ctrl Pts',(-27.110991898551,24.1809217806606,-75.));
#71708=CARTESIAN_POINT('Ctrl Pts',(-27.1089458950028,24.2051214179296,-75.));
#71709=CARTESIAN_POINT('Ctrl Pts',(-27.1066365391915,24.2293101033335,-75.));
#71710=CARTESIAN_POINT('Ctrl Pts',(-27.1040658591694,24.253484904205,-75.));
#71711=CARTESIAN_POINT('Ctrl Pts',(-27.1016965285288,24.2757662056281,-75.));
#71712=CARTESIAN_POINT('Ctrl Pts',(-27.0991044565744,24.2980408276541,-75.));
#71713=CARTESIAN_POINT('Ctrl Pts',(-27.0962953485937,24.3202756476038,-75.));
#71714=CARTESIAN_POINT('Ctrl Pts',(-27.0821928071296,24.4319009295238,-75.));
#71715=CARTESIAN_POINT('Ctrl Pts',(-27.0626133321251,24.5426515225154,-75.));
#71716=CARTESIAN_POINT('Ctrl Pts',(-27.0378716668943,24.6522326854476,-75.));
#71717=CARTESIAN_POINT('Ctrl Pts',(-27.0126702012133,24.7638503106628,-75.));
#71718=CARTESIAN_POINT('Ctrl Pts',(-26.9821127731921,24.8742552769071,-75.));
#71719=CARTESIAN_POINT('Ctrl Pts',(-26.9464772616989,24.9831449167715,-75.));
#71720=CARTESIAN_POINT('Ctrl Pts',(-26.9101118870068,25.094264762898,-75.));
#71721=CARTESIAN_POINT('Ctrl Pts',(-26.8684581529784,25.2038073287541,-75.));
#71722=CARTESIAN_POINT('Ctrl Pts',(-26.8217568024216,25.3114493823763,-75.));
#71723=CARTESIAN_POINT('Ctrl Pts',(-26.7832118857427,25.4002916522152,-75.));
#71724=CARTESIAN_POINT('Ctrl Pts',(-26.7412274435804,25.4878394728692,-75.));
#71725=CARTESIAN_POINT('Ctrl Pts',(-26.6959129135712,25.5739046319901,-75.));
#71726=CARTESIAN_POINT('Ctrl Pts',(-26.6858732433753,25.5929728163619,-75.));
#71727=CARTESIAN_POINT('Ctrl Pts',(-26.6756700236405,25.6119681875733,-75.));
#71728=CARTESIAN_POINT('Ctrl Pts',(-26.6653042992829,25.63088863441,-75.));
#71729=CARTESIAN_POINT('Ctrl Pts',(-26.6561483093346,25.6476009658473,-75.));
#71730=CARTESIAN_POINT('Ctrl Pts',(-26.6468698353721,25.6642469346371,-75.));
#71731=CARTESIAN_POINT('Ctrl Pts',(-26.6374723605576,25.6808210785559,-75.));
#71732=CARTESIAN_POINT('Ctrl Pts',(-26.5781216176399,25.7854968317996,-75.));
#71733=CARTESIAN_POINT('Ctrl Pts',(-26.5139994851696,25.8873614230389,-75.));
#71734=CARTESIAN_POINT('Ctrl Pts',(-26.4453803727087,25.9860816677649,-75.));
#71735=CARTESIAN_POINT('Ctrl Pts',(-26.3762554483936,26.0855296087295,-75.));
#71736=CARTESIAN_POINT('Ctrl Pts',(-26.3025666925354,26.1817875091273,-75.));
#71737=CARTESIAN_POINT('Ctrl Pts',(-26.2245441756349,26.2745003905634,-75.));
#71738=CARTESIAN_POINT('Ctrl Pts',(-26.1893020912291,26.3163779833772,-75.));
#71739=CARTESIAN_POINT('Ctrl Pts',(-26.1531751604097,26.3575320336574,-75.));
#71740=CARTESIAN_POINT('Ctrl Pts',(-26.1161815127994,26.3979281671849,-75.));
#71741=CARTESIAN_POINT('Ctrl Pts',(-26.0949645293092,26.4210965799662,-75.));
#71742=CARTESIAN_POINT('Ctrl Pts',(-26.0734574109817,26.4440206775451,-75.));
#71743=CARTESIAN_POINT('Ctrl Pts',(-26.0516898669499,26.4666667346163,-75.));
#71744=CARTESIAN_POINT('Ctrl Pts',(-25.9662054925696,26.5556011600195,-75.));
#71745=CARTESIAN_POINT('Ctrl Pts',(-25.8766542573217,26.6403121959665,-75.));
#71746=CARTESIAN_POINT('Ctrl Pts',(-25.7832911788552,26.7204449987284,-75.));
#71747=CARTESIAN_POINT('Ctrl Pts',(-25.6911368051049,26.7995403796505,-75.));
#71748=CARTESIAN_POINT('Ctrl Pts',(-25.5952681674086,26.8741760556854,-75.));
#71749=CARTESIAN_POINT('Ctrl Pts',(-25.4958878475418,26.9439845596524,-75.0000000000001));
#71750=CARTESIAN_POINT('Ctrl Pts',(-25.4316916215268,26.9890784223451,-75.0000000000001));
#71751=CARTESIAN_POINT('Ctrl Pts',(-25.3660292286572,27.0321574883894,-75.0000000000001));
#71752=CARTESIAN_POINT('Ctrl Pts',(-25.2989470070244,27.0731145261455,-75.0000000000001));
#71753=CARTESIAN_POINT('Ctrl Pts',(-21.2666653996577,20.3445903493589,-75.4118502628812));
#71754=CARTESIAN_POINT('Ctrl Pts',(-20.1976516050523,21.1060288780026,-75.3455104329369));
#71755=CARTESIAN_POINT('Ctrl Pts',(-18.9008443259664,23.7684865465132,-75.2128749658675));
#71756=CARTESIAN_POINT('Ctrl Pts',(-21.2264059286695,27.5877942357118,-75.013943861673));
#71757=CARTESIAN_POINT('Ctrl Pts',(-25.688658539591,27.6837853569551,-74.8150569502983));
#71758=CARTESIAN_POINT('Ctrl Pts',(-28.1849582354078,23.9876330729271,-74.6161700389233));
#71759=CARTESIAN_POINT('Ctrl Pts',(-26.4228527910817,19.886306014703,-74.4172831275484));
#71760=CARTESIAN_POINT('Ctrl Pts',(-22.0208084558691,19.1535567442735,-74.2183962161735));
#71761=CARTESIAN_POINT('Ctrl Pts',(-19.0243327220968,22.4600869091669,-74.0195093047986));
#71762=CARTESIAN_POINT('Ctrl Pts',(-20.1867198546258,26.7688693666575,-73.8206223934237));
#71763=CARTESIAN_POINT('Ctrl Pts',(-24.439947370569,28.1197603121436,-73.6217354820488));
#71764=CARTESIAN_POINT('Ctrl Pts',(-27.8756000908746,25.2717963687883,-73.4228485706739));
#71765=CARTESIAN_POINT('Ctrl Pts',(-27.3366360814689,20.8418079302662,-73.2239616592991));
#71766=CARTESIAN_POINT('Ctrl Pts',(-23.3183008240058,18.9006883998381,-73.0250747479242));
#71767=CARTESIAN_POINT('Ctrl Pts',(-19.5131125903956,21.2321039860555,-72.8261878365494));
#71768=CARTESIAN_POINT('Ctrl Pts',(-19.4177120435377,25.6937121854946,-72.6273009251744));
#71769=CARTESIAN_POINT('Ctrl Pts',(-23.1197666849278,28.1856570601434,-72.4284140137995));
#71770=CARTESIAN_POINT('Ctrl Pts',(-27.2174008641755,26.4180611767357,-72.2295271024246));
#71771=CARTESIAN_POINT('Ctrl Pts',(-27.9452368903513,22.0151907171623,-72.0306401910497));
#71772=CARTESIAN_POINT('Ctrl Pts',(-24.6344547962064,19.022912750906,-71.8317532796748));
#71773=CARTESIAN_POINT('Ctrl Pts',(-20.3273828139243,20.1908757445163,-71.6328663683));
#71774=CARTESIAN_POINT('Ctrl Pts',(-18.9818548120982,24.4458214122759,-71.433979456925));
#71775=CARTESIAN_POINT('Ctrl Pts',(-21.8342969973335,27.8778150860887,-71.2350925455501));
#71776=CARTESIAN_POINT('Ctrl Pts',(-26.2635568195445,27.3331457550989,-71.0362056341753));
#71777=CARTESIAN_POINT('Ctrl Pts',(-28.1995200568178,23.3123182533585,-70.8373187228003));
#71778=CARTESIAN_POINT('Ctrl Pts',(-25.8632006285602,19.510132198389,-70.6384318114255));
#71779=CARTESIAN_POINT('Ctrl Pts',(-21.4014780064369,19.4204741742239,-70.4395449000505));
#71780=CARTESIAN_POINT('Ctrl Pts',(-18.9142969861975,23.1257323182947,-70.2406579886757));
#71781=CARTESIAN_POINT('Ctrl Pts',(-20.687166048478,27.221088542356,-70.0417710773009));
#71782=CARTESIAN_POINT('Ctrl Pts',(-25.0909688389096,27.9432577096414,-69.8428841659259));
#71783=CARTESIAN_POINT('Ctrl Pts',(-28.0789839743286,24.6286275830399,-69.6439972545512));
#71784=CARTESIAN_POINT('Ctrl Pts',(-26.9054788870104,20.3230622157861,-69.445110343176));
#71785=CARTESIAN_POINT('Ctrl Pts',(-22.648805255472,18.9830111280192,-69.2462234318014));
#71786=CARTESIAN_POINT('Ctrl Pts',(-19.2204852406392,21.8398676521317,-69.0473365204262));
#71787=CARTESIAN_POINT('Ctrl Pts',(-19.7708542625673,26.268422863778,-68.8484496090516));
#71788=CARTESIAN_POINT('Ctrl Pts',(-23.7941698536879,28.1992100031105,-68.6495626976765));
#71789=CARTESIAN_POINT('Ctrl Pts',(-27.5933461066773,25.8579993927866,-68.4506757863017));
#71790=CARTESIAN_POINT('Ctrl Pts',(-27.6772621620609,21.3961650817951,-68.2517888749267));
#71791=CARTESIAN_POINT('Ctrl Pts',(-23.9688062798515,18.9137545007584,-68.0529019635519));
#71792=CARTESIAN_POINT('Ctrl Pts',(-19.8757349905908,20.6918924999483,-67.854015052177));
#71793=CARTESIAN_POINT('Ctrl Pts',(-19.1592337738934,25.0966210193459,-67.6551281408021));
#71794=CARTESIAN_POINT('Ctrl Pts',(-22.4777064986191,28.0803680090189,-67.4562412294273));
#71795=CARTESIAN_POINT('Ctrl Pts',(-26.7817580908333,26.901322965483,-67.2573543180523));
#71796=CARTESIAN_POINT('Ctrl Pts',(-28.1163300606876,22.6429283172139,-67.0584674066776));
#71797=CARTESIAN_POINT('Ctrl Pts',(-25.255063920929,19.2182876936448,-66.8595804953024));
#71798=CARTESIAN_POINT('Ctrl Pts',(-20.8272206586329,19.7743554661939,-66.6606935839279));
#71799=CARTESIAN_POINT('Ctrl Pts',(-18.9016128126505,23.8001524986608,-66.4618066725527));
#71800=CARTESIAN_POINT('Ctrl Pts',(-21.2477107288177,27.5963126495084,-66.262919761178));
#71801=CARTESIAN_POINT('Ctrl Pts',(-25.7096493384775,27.6744866014112,-66.0640328498029));
#71802=CARTESIAN_POINT('Ctrl Pts',(-28.1872853693601,23.9628391206286,-65.8651459384281));
#71803=CARTESIAN_POINT('Ctrl Pts',(-26.4038813779779,19.8720595461892,-65.6662590270532));
#71804=CARTESIAN_POINT('Ctrl Pts',(-21.998234424688,19.1612274660918,-65.4673721156783));
#71805=CARTESIAN_POINT('Ctrl Pts',(-19.0187605223013,22.4835372933243,-65.2684852043034));
#71806=CARTESIAN_POINT('Ctrl Pts',(-20.2033435693833,26.7860679820812,-65.0695982929285));
#71807=CARTESIAN_POINT('Ctrl Pts',(-24.4634521817448,28.1151586238398,-64.8707113815536));
#71808=CARTESIAN_POINT('Ctrl Pts',(-27.8844077422721,25.2494876071271,-64.6718244701788));
#71809=CARTESIAN_POINT('Ctrl Pts',(-27.3226421400403,20.8223636274675,-64.4729375588038));
#71810=CARTESIAN_POINT('Ctrl Pts',(-23.2943703336322,18.9019382639541,-64.2740506474291));
#71811=CARTESIAN_POINT('Ctrl Pts',(-19.5012325720103,21.2529196004361,-64.075163736054));
#71812=CARTESIAN_POINT('Ctrl Pts',(-19.4288008530583,25.7149551190328,-63.8762768246794));
#71813=CARTESIAN_POINT('Ctrl Pts',(-23.143633785296,28.1878124963781,-63.6773899133043));
#71814=CARTESIAN_POINT('Ctrl Pts',(-27.2321148698893,26.399145466422,-63.4785030019295));
#71815=CARTESIAN_POINT('Ctrl Pts',(-27.937276636128,21.992587375739,-63.2796160905546));
#71816=CARTESIAN_POINT('Ctrl Pts',(-24.6111352086973,19.0173914951528,-63.0807291791796));
#71817=CARTESIAN_POINT('Ctrl Pts',(-20.3101325491186,20.2075105839101,-62.8818422678048));
#71818=CARTESIAN_POINT('Ctrl Pts',(-18.9865254366552,24.4693261049017,-62.6829553564298));
#71819=CARTESIAN_POINT('Ctrl Pts',(-21.8565965842846,27.8865909367042,-62.484068445055));
#71820=CARTESIAN_POINT('Ctrl Pts',(-26.2829939492395,27.319128435169,-62.28518153368));
#71821=CARTESIAN_POINT('Ctrl Pts',(-28.1982336497336,23.288388526321,-62.0862946223052));
#71822=CARTESIAN_POINT('Ctrl Pts',(-25.8423727865607,19.4982794360047,-61.8874077109303));
#71823=CARTESIAN_POINT('Ctrl Pts',(-21.3802477489149,19.4315900699627,-61.6885207995554));
#71824=CARTESIAN_POINT('Ctrl Pts',(-18.9121731205785,23.149602301262,-61.4896338881805));
#71825=CARTESIAN_POINT('Ctrl Pts',(-20.7061002267723,27.2357781247906,-61.2907469768056));
#71826=CARTESIAN_POINT('Ctrl Pts',(-25.1135621568407,27.9352684093035,-61.0918600654307));
#71827=CARTESIAN_POINT('Ctrl Pts',(-28.0844750881974,24.6053008903289,-60.8929731540559));
#71828=CARTESIAN_POINT('Ctrl Pts',(-26.8888219288037,20.3058333831184,-60.6940862426809));
#71829=CARTESIAN_POINT('Ctrl Pts',(-22.6253065574715,18.9877119920681,-60.4951993313061));
#71830=CARTESIAN_POINT('Ctrl Pts',(-19.211738113964,21.8621785172896,-60.2963124199312));
#71831=CARTESIAN_POINT('Ctrl Pts',(-19.7848965749885,26.2878419366748,-60.0974255085563));
#71832=CARTESIAN_POINT('Ctrl Pts',(-23.8180979106871,28.1978928021876,-59.8985385971813));
#71833=CARTESIAN_POINT('Ctrl Pts',(-27.6051720526345,25.8371563140293,-59.6996516858066));
#71834=CARTESIAN_POINT('Ctrl Pts',(-27.6661189553175,21.3749491473704,-59.5007647744315));
#71835=CARTESIAN_POINT('Ctrl Pts',(-23.9449335826159,18.9116613555929,-59.3018778630568));
#71836=CARTESIAN_POINT('Ctrl Pts',(-19.8610697875519,20.7108455669771,-59.1029909516818));
#71837=CARTESIAN_POINT('Ctrl Pts',(-19.1672521432397,25.1192040369259,-58.904104040307));
#71838=CARTESIAN_POINT('Ctrl Pts',(-22.5010402387668,28.0858290987175,-58.705217128932));
#71839=CARTESIAN_POINT('Ctrl Pts',(-26.7989654729617,26.8846438488917,-58.5063302175572));
#71840=CARTESIAN_POINT('Ctrl Pts',(-28.111598959566,22.6194356883239,-58.3074433061823));
#71841=CARTESIAN_POINT('Ctrl Pts',(-25.2327418173569,19.2095692865597,-58.1085563948074));
#71842=CARTESIAN_POINT('Ctrl Pts',(-20.8078196731909,19.7884227578258,-57.9096694834325));
#71843=CARTESIAN_POINT('Ctrl Pts',(-18.9029608060273,23.8240788407097,-57.7107825720576));
#71844=CARTESIAN_POINT('Ctrl Pts',(-21.2685690093912,27.6081117622506,-57.5118956606827));
#71845=CARTESIAN_POINT('Ctrl Pts',(-25.7308509148911,27.6633161006365,-57.3130087493078));
#71846=CARTESIAN_POINT('Ctrl Pts',(-28.189347790487,23.9389637494465,-57.1141218379329));
#71847=CARTESIAN_POINT('Ctrl Pts',(-26.384909453667,19.8574187464186,-56.915234926558));
#71848=CARTESIAN_POINT('Ctrl Pts',(-21.975661744827,19.1692748913867,-56.7163480151832));
#71849=CARTESIAN_POINT('Ctrl Pts',(-19.013329465835,22.5068780421479,-56.5174611038082));
#71850=CARTESIAN_POINT('Ctrl Pts',(-20.2200448167264,26.8032538852337,-56.3185741924334));
#71851=CARTESIAN_POINT('Ctrl Pts',(-24.4869387026215,28.1103972934484,-56.1196872810584));
#71852=CARTESIAN_POINT('Ctrl Pts',(-27.8930974153251,25.2271543021274,-55.9208003696836));
#71853=CARTESIAN_POINT('Ctrl Pts',(-27.3085498924968,20.8029807616021,-55.7219134583087));
#71854=CARTESIAN_POINT('Ctrl Pts',(-23.2704457461589,18.9033170475574,-55.5230265469337));
#71855=CARTESIAN_POINT('Ctrl Pts',(-19.4894603120249,21.2737930482783,-55.3241396355589));
#71856=CARTESIAN_POINT('Ctrl Pts',(-19.4399986293641,25.7361423023235,-55.125252724184));
#71857=CARTESIAN_POINT('Ctrl Pts',(-23.1675117908829,28.1898441900499,-54.9263658128092));
#71858=CARTESIAN_POINT('Ctrl Pts',(-27.2467312421439,26.3801547162498,-54.7274789014342));
#71859=CARTESIAN_POINT('Ctrl Pts',(-27.9292001682125,21.970025070981,-54.5285919900594));
#71860=CARTESIAN_POINT('Ctrl Pts',(-24.5877874898543,19.0119904809134,-54.3297050786844));
#71861=CARTESIAN_POINT('Ctrl Pts',(-20.2929681534049,20.2242339343449,-54.1308181673096));
#71862=CARTESIAN_POINT('Ctrl Pts',(-18.9913169884309,24.4928064788673,-53.9319312559346));
#71863=CARTESIAN_POINT('Ctrl Pts',(-21.8789410537244,27.8952518613337,-53.7330443445599));
#71864=CARTESIAN_POINT('Ctrl Pts',(-26.3023586634269,27.3050112550531,-53.5341574331848));
#71865=CARTESIAN_POINT('Ctrl Pts',(-28.1968240781874,23.2644657330469,-53.3352705218101));
#71866=CARTESIAN_POINT('Ctrl Pts',(-25.8214842060198,19.4865340482728,-53.136383610435));
#71867=CARTESIAN_POINT('Ctrl Pts',(-21.3590749938369,19.442815103254,-52.9374966990602));
#71868=CARTESIAN_POINT('Ctrl Pts',(-18.9101721577264,23.1734829017077,-52.7386097876853));
#71869=CARTESIAN_POINT('Ctrl Pts',(-20.7251097713536,27.2503700453221,-52.5397228763104));
#71870=CARTESIAN_POINT('Ctrl Pts',(-25.1361140491286,27.9271629121431,-52.3408359649356));
#71871=CARTESIAN_POINT('Ctrl Pts',(-28.0898460512646,24.5819462401343,-52.1419490535606));
#71872=CARTESIAN_POINT('Ctrl Pts',(-26.8720765029738,20.2886905232705,-51.9430621421858));
#71873=CARTESIAN_POINT('Ctrl Pts',(-22.6018323693044,18.9925337572925,-51.7441752308108));
#71874=CARTESIAN_POINT('Ctrl Pts',(-19.2031059521021,21.8845341141631,-51.545288319436));
#71875=CARTESIAN_POINT('Ctrl Pts',(-19.7990386642963,26.3071884671128,-51.3464014080611));
#71876=CARTESIAN_POINT('Ctrl Pts',(-23.8420188701422,28.196452445033,-51.1475144966862));
#71877=CARTESIAN_POINT('Ctrl Pts',(-27.6168905486605,25.8162526353847,-50.9486275853114));
#71878=CARTESIAN_POINT('Ctrl Pts',(-27.6548666836312,21.3537908555707,-50.7497406739364));
#71879=CARTESIAN_POINT('Ctrl Pts',(-23.9210504268616,18.9096911268747,-50.5508537625616));
#71880=CARTESIAN_POINT('Ctrl Pts',(-19.8465023429102,20.7298738744846,-50.3519668511866));
#71881=CARTESIAN_POINT('Ctrl Pts',(-19.1753866562207,25.141745479394,-50.1530799398118));
#71882=CARTESIAN_POINT('Ctrl Pts',(-22.524401781634,28.0911700017174,-49.9541930284368));
#71883=CARTESIAN_POINT('Ctrl Pts',(-26.8160867685523,26.8678763754001,-49.755306117062));
#71884=CARTESIAN_POINT('Ctrl Pts',(-28.1067469888788,22.5959677248325,-49.556419205687));
#71885=CARTESIAN_POINT('Ctrl Pts',(-25.2103751300742,19.2009659017617,-49.3575322943122));
#71886=CARTESIAN_POINT('Ctrl Pts',(-20.7884913585431,19.802589732904,-49.1586453829372));
#71887=CARTESIAN_POINT('Ctrl Pts',(-18.9044319464049,23.8479979267284,-48.9597584715625));
#71888=CARTESIAN_POINT('Ctrl Pts',(-21.2894877515194,27.6198033471629,-48.7608715601874));
#71889=CARTESIAN_POINT('Ctrl Pts',(-25.7519947083708,27.6520366091907,-48.5619846488127));
#71890=CARTESIAN_POINT('Ctrl Pts',(-28.1912872818085,23.9150780779383,-48.3630977374377));
#71891=CARTESIAN_POINT('Ctrl Pts',(-26.3658624147475,19.8428758017929,-48.1642108260628));
#71892=CARTESIAN_POINT('Ctrl Pts',(-21.953130789511,19.1774384067162,-47.965323914688));
#71893=CARTESIAN_POINT('Ctrl Pts',(-19.0080186317479,22.5302464389967,-47.7664370033131));
#71894=CARTESIAN_POINT('Ctrl Pts',(-20.2368343101097,26.8203535882111,-47.5675500919381));
#71895=CARTESIAN_POINT('Ctrl Pts',(-24.5104004025703,28.1055151253339,-47.3686631805633));
#71896=CARTESIAN_POINT('Ctrl Pts',(-27.9016720088104,25.2047765614785,-47.1697762691884));
#71897=CARTESIAN_POINT('Ctrl Pts',(-27.2943580551114,20.7836706947557,-46.9708893578135));
#71898=CARTESIAN_POINT('Ctrl Pts',(-23.2465285731905,18.9048189687216,-46.7720024464386));
#71899=CARTESIAN_POINT('Ctrl Pts',(-19.4777956575895,21.2947268192451,-46.5731155350638));
#71900=CARTESIAN_POINT('Ctrl Pts',(-19.4513053218883,25.7572715624655,-46.3742286236887));
#71901=CARTESIAN_POINT('Ctrl Pts',(-23.1913999385863,28.1917529407624,-46.175341712314));
#71902=CARTESIAN_POINT('Ctrl Pts',(-27.261249662668,26.3610889774635,-45.976454800939));
#71903=CARTESIAN_POINT('Ctrl Pts',(-27.9210076640546,21.9475046401323,-45.7775678895642));
#71904=CARTESIAN_POINT('Ctrl Pts',(-24.5644122777257,19.0067097245348,-45.5786809781893));
#71905=CARTESIAN_POINT('Ctrl Pts',(-20.2758900713606,20.2410454198139,-45.3797940668144));
#71906=CARTESIAN_POINT('Ctrl Pts',(-18.9962293458869,24.5162618764169,-45.1809071554395));
#71907=CARTESIAN_POINT('Ctrl Pts',(-21.901329810678,27.9037976493055,-44.9820202440646));
#71908=CARTESIAN_POINT('Ctrl Pts',(-26.3216504504911,27.2907945788645,-44.7831333326896));
#71909=CARTESIAN_POINT('Ctrl Pts',(-28.1952913787241,23.2405505127397,-44.5842464213149));
#71910=CARTESIAN_POINT('Ctrl Pts',(-25.8005354408843,19.4748963436331,-44.3853595099398));
#71911=CARTESIAN_POINT('Ctrl Pts',(-21.3379603020264,19.4541489781311,-44.1864725985652));
#71912=CARTESIAN_POINT('Ctrl Pts',(-18.908294150784,23.1973734860435,-43.9875856871901));
#71913=CARTESIAN_POINT('Ctrl Pts',(-20.7441941784308,27.2648639176997,-43.7886987758153));
#71914=CARTESIAN_POINT('Ctrl Pts',(-25.1586239182123,27.9189414327251,-43.5898118644403));
#71915=CARTESIAN_POINT('Ctrl Pts',(-28.0950967211891,24.5585642514394,-43.3909249530655));
#71916=CARTESIAN_POINT('Ctrl Pts',(-26.8552430532619,20.2716340904436,-43.1920380416906));
#71917=CARTESIAN_POINT('Ctrl Pts',(-22.5783833130001,18.9974762959544,-42.9931511303156));
#71918=CARTESIAN_POINT('Ctrl Pts',(-19.1945889837971,21.9069338503419,-42.7942642189409));
#71919=CARTESIAN_POINT('Ctrl Pts',(-19.813280155743,26.3264619424445,-42.5953773075658));
#71920=CARTESIAN_POINT('Ctrl Pts',(-23.8659320981805,28.194888969809,-42.3964903961911));
#71921=CARTESIAN_POINT('Ctrl Pts',(-27.6285012842304,25.7952889107751,-42.1976034848161));
#71922=CARTESIAN_POINT('Ctrl Pts',(-27.6435056451722,21.332690767061,-41.9987165734413));
#71923=CARTESIAN_POINT('Ctrl Pts',(-23.8971574454602,18.9078438668127,-41.7998296620662));
#71924=CARTESIAN_POINT('Ctrl Pts',(-19.8320330426836,20.7489769182455,-41.6009427506916));
#71925=CARTESIAN_POINT('Ctrl Pts',(-19.1836370972827,25.1642447494326,-41.4020558393165));
#71926=CARTESIAN_POINT('Ctrl Pts',(-22.5477905081707,28.0963905764916,-41.2031689279418));
#71927=CARTESIAN_POINT('Ctrl Pts',(-26.8331215239135,26.8510209893242,-41.0042820165667));
#71928=CARTESIAN_POINT('Ctrl Pts',(-28.1017742771965,22.5725250486092,-40.805395105192));
#71929=CARTESIAN_POINT('Ctrl Pts',(-25.1879644517681,19.192477767229,-40.6065081938169));
#71930=CARTESIAN_POINT('Ctrl Pts',(-20.7692362268642,19.8168560160224,-40.4076212824422));
#71931=CARTESIAN_POINT('Ctrl Pts',(-18.9060261948002,23.8719091228934,-40.2087343710672));
#71932=CARTESIAN_POINT('Ctrl Pts',(-21.3104664008835,27.631387094434,-40.0098474596923));
#71933=CARTESIAN_POINT('Ctrl Pts',(-25.7730801586343,27.6406484259655,-39.8109605483174));
#71934=CARTESIAN_POINT('Ctrl Pts',(-28.1931037919306,23.8911827390422,-39.6120736369426));
#71935=CARTESIAN_POINT('Ctrl Pts',(-26.3467407659406,19.8284310976806,-39.4131867255677));
#71936=CARTESIAN_POINT('Ctrl Pts',(-21.9306421557803,19.1857177957581,-39.2142998141928));
#71937=CARTESIAN_POINT('Ctrl Pts',(-19.0028281607701,22.5536418646396,-39.0154129028179));
#71938=CARTESIAN_POINT('Ctrl Pts',(-20.2537116046342,26.8373666378943,-38.816525991443));
#71939=CARTESIAN_POINT('Ctrl Pts',(-24.5338366598877,28.1005122488671,-38.6176390800681));
#71940=CARTESIAN_POINT('Ctrl Pts',(-27.910131295513,25.1823549781609,-38.4187521686932));
#71941=CARTESIAN_POINT('Ctrl Pts',(-27.2800670039488,20.7644339386194,-38.2198652573183));
#71942=CARTESIAN_POINT('Ctrl Pts',(-23.2226194484999,18.9064439876479,-38.0209783459435));
#71943=CARTESIAN_POINT('Ctrl Pts',(-19.4662389178021,21.3157203586197,-37.8220914345685));
#71944=CARTESIAN_POINT('Ctrl Pts',(-19.4627206310189,25.7783423395616,-37.6232045231937));
#71945=CARTESIAN_POINT('Ctrl Pts',(-23.2152975954025,28.1935386979362,-37.4243176118188));
#71946=CARTESIAN_POINT('Ctrl Pts',(-27.2756697467429,26.3419487552794,-37.2254307004438));
#71947=CARTESIAN_POINT('Ctrl Pts',(-27.912699340745,21.9250266799544,-37.026543789069));
#71948=CARTESIAN_POINT('Ctrl Pts',(-24.5410101917235,19.0015493659496,-36.827656877694));
#71949=CARTESIAN_POINT('Ctrl Pts',(-20.258898755532,20.2579445948353,-36.6287699663193));
#71950=CARTESIAN_POINT('Ctrl Pts',(-19.0012623788527,24.5396916760138,-36.4298830549443));
#71951=CARTESIAN_POINT('Ctrl Pts',(-21.9237622618732,27.9122280741679,-36.2309961435695));
#71952=CARTESIAN_POINT('Ctrl Pts',(-26.3408687992257,27.2764787833259,-36.0321092321945));
#71953=CARTESIAN_POINT('Ctrl Pts',(-28.1936355919582,23.2166434991209,-35.8332223208196));
#71954=CARTESIAN_POINT('Ctrl Pts',(-25.7795270462683,19.4633666304692,-35.6343354094447));
#71955=CARTESIAN_POINT('Ctrl Pts',(-21.3169042329942,19.4655913942613,-35.4354484980699));
#71956=CARTESIAN_POINT('Ctrl Pts',(-18.906539149516,23.221273421201,-35.2365615866949));
#71957=CARTESIAN_POINT('Ctrl Pts',(-20.7633529422927,27.2792593578551,-35.0376746753201));
#71958=CARTESIAN_POINT('Ctrl Pts',(-25.1810911676103,27.9106041889076,-34.8387877639452));
#71959=CARTESIAN_POINT('Ctrl Pts',(-28.1002269588351,24.5351555438356,-34.6399008525703));
#71960=CARTESIAN_POINT('Ctrl Pts',(-26.8383220257315,20.2546645366102,-34.4410139411954));
#71961=CARTESIAN_POINT('Ctrl Pts',(-22.5549600099273,19.0025394770835,-34.2421270298205));
#71962=CARTESIAN_POINT('Ctrl Pts',(-19.1861874347372,21.9293771322627,-34.0432401184457));
#71963=CARTESIAN_POINT('Ctrl Pts',(-19.827620671948,26.3456618519484,-33.8443532070707));
#71964=CARTESIAN_POINT('Ctrl Pts',(-23.8898369611334,28.1932024179458,-33.6454662956958));
#71965=CARTESIAN_POINT('Ctrl Pts',(-27.6400039516757,25.7742656957109,-33.446579384321));
#71966=CARTESIAN_POINT('Ctrl Pts',(-27.6320361409929,21.3116494409653,-33.247692472946));
#71967=CARTESIAN_POINT('Ctrl Pts',(-23.8732552715437,18.9061196243572,-33.0488055615712));
#71968=CARTESIAN_POINT('Ctrl Pts',(-19.8176622702888,20.768154192055,-32.8499186501963));
#71969=CARTESIAN_POINT('Ctrl Pts',(-19.1920032478,25.1867012508411,-32.6510317388214));
#71970=CARTESIAN_POINT('Ctrl Pts',(-22.5712057986073,28.1014906847019,-32.4521448274465));
#71971=CARTESIAN_POINT('Ctrl Pts',(-26.8500692876472,26.8340781373091,-32.2532579160716));
#71972=CARTESIAN_POINT('Ctrl Pts',(-28.0966809562897,22.5491082808535,-32.0543710046967));
#71973=CARTESIAN_POINT('Ctrl Pts',(-25.1655103762915,19.1841051078859,-31.8554840933218));
#71974=CARTESIAN_POINT('Ctrl Pts',(-20.7500547883893,19.8312212291436,-31.656597181947));
#71975=CARTESIAN_POINT('Ctrl Pts',(-18.9077435089677,23.8958117955898,-31.457710270572));
#71976=CARTESIAN_POINT('Ctrl Pts',(-21.3315044015777,27.6428626971101,-31.2588233591972));
#71977=CARTESIAN_POINT('Ctrl Pts',(-25.7941067069455,27.6291518527325,-31.0599364478223));
#71978=CARTESIAN_POINT('Ctrl Pts',(-28.1947972727182,23.8672783659527,-30.8610495364474));
#71979=CARTESIAN_POINT('Ctrl Pts',(-26.3275450139443,19.8140850168471,-30.6621626250725));
#71980=CARTESIAN_POINT('Ctrl Pts',(-21.9081964395532,19.1941128391196,-30.4632757136976));
#71981=CARTESIAN_POINT('Ctrl Pts',(-18.9977581904422,22.5770636991292,-30.2643888023227));
#71982=CARTESIAN_POINT('Ctrl Pts',(-20.270676253074,26.8542925834601,-30.0655018909478));
#71983=CARTESIAN_POINT('Ctrl Pts',(-24.5572468535441,28.0953887966177,-29.8666149795729));
#71984=CARTESIAN_POINT('Ctrl Pts',(-27.9184750512729,25.1598901463163,-29.667728068198));
#71985=CARTESIAN_POINT('Ctrl Pts',(-27.2656771177025,20.7452710029411,-29.4688411568231));
#71986=CARTESIAN_POINT('Ctrl Pts',(-23.1987190056467,18.9081920612753,-29.2699542454482));
#71987=CARTESIAN_POINT('Ctrl Pts',(-19.4547903989006,21.3367731101012,-29.0710673340734));
#71988=CARTESIAN_POINT('Ctrl Pts',(-19.4742442542653,25.7993540752649,-28.8721804226984));
#71989=CARTESIAN_POINT('Ctrl Pts',(-23.2392041280753,28.1952014142512,-28.6732935113236));
#71990=CARTESIAN_POINT('Ctrl Pts',(-27.2899911122557,26.3227345568877,-28.4744065999487));
#71991=CARTESIAN_POINT('Ctrl Pts',(-27.9042754184428,21.9025917860827,-28.2755196885738));
#71992=CARTESIAN_POINT('Ctrl Pts',(-24.5175818519714,18.9965095419007,-28.0766327771989));
#71993=CARTESIAN_POINT('Ctrl Pts',(-20.2419946561664,20.2749310116035,-27.877745865824));
#71994=CARTESIAN_POINT('Ctrl Pts',(-19.0064159539593,24.5630952567998,-27.6788589544491));
#71995=CARTESIAN_POINT('Ctrl Pts',(-21.9462378128801,27.9205429125257,-27.4799720430743));
#71996=CARTESIAN_POINT('Ctrl Pts',(-26.36001320037,27.2620642477869,-27.2810851316994));
#71997=CARTESIAN_POINT('Ctrl Pts',(-28.1918567617659,23.1927453256942,-27.0821982203245));
#71998=CARTESIAN_POINT('Ctrl Pts',(-25.758459578866,19.451945214303,-26.8833113089496));
#71999=CARTESIAN_POINT('Ctrl Pts',(-21.2959073446981,19.4771420484359,-26.6844243975747));
#72000=CARTESIAN_POINT('Ctrl Pts',(-18.9049072004276,23.245182073864,-26.4855374861998));
#72001=CARTESIAN_POINT('Ctrl Pts',(-20.7825855552577,27.2935559843285,-26.2866505748249));
#72002=CARTESIAN_POINT('Ctrl Pts',(-25.2035152019707,27.9021514016165,-26.08776366345));
#72003=CARTESIAN_POINT('Ctrl Pts',(-28.105236628258,24.5117207376222,-25.8888767520751));
#72004=CARTESIAN_POINT('Ctrl Pts',(-26.8213138687676,20.2377823114409,-25.6899898407003));
#72005=CARTESIAN_POINT('Ctrl Pts',(-22.5315630807722,19.007723166512,-25.4911029293253));
#72006=CARTESIAN_POINT('Ctrl Pts',(-19.1779015275521,21.9518633652088,-25.2922160179505));
#72007=CARTESIAN_POINT('Ctrl Pts',(-19.842059832907,26.3647876868526,-25.0933291065755));
#72008=CARTESIAN_POINT('Ctrl Pts',(-23.9137328255541,28.1913928341347,-24.8944421952007));
#72009=CARTESIAN_POINT('Ctrl Pts',(-27.6513982461906,25.7531835472795,-24.6955552838258));
#72010=CARTESIAN_POINT('Ctrl Pts',(-27.6204584750198,21.2906674348507,-24.4966683724509));
#72011=CARTESIAN_POINT('Ctrl Pts',(-23.8493445384875,18.9045184451978,-24.297781461076));
#72012=CARTESIAN_POINT('Ctrl Pts',(-19.8033904065325,20.7874051877409,-24.0988945497011));
#72013=CARTESIAN_POINT('Ctrl Pts',(-19.200484886081,25.209114388552,-23.9000076383262));
#72014=CARTESIAN_POINT('Ctrl Pts',(-22.5946470324697,28.1064701912023,-23.7011207269513));
#72015=CARTESIAN_POINT('Ctrl Pts',(-26.8669296106604,26.8170482683175,-23.5022338155764));
#72016=CARTESIAN_POINT('Ctrl Pts',(-28.0914671611242,22.5257180420785,-23.3033469042016));
#72017=CARTESIAN_POINT('Ctrl Pts',(-25.1430134986476,19.1758481455965,-23.1044599928266));
#72018=CARTESIAN_POINT('Ctrl Pts',(-20.7309475514009,19.8456849916087,-22.9055730814518));
#72019=CARTESIAN_POINT('Ctrl Pts',(-18.9095838434007,23.919705311429,-22.7066861700768));
#72020=CARTESIAN_POINT('Ctrl Pts',(-21.3526011961228,27.654229851103,-22.507799258702));
#72021=CARTESIAN_POINT('Ctrl Pts',(-25.8150737961289,27.6175471941357,-22.3089123473271));
#72022=CARTESIAN_POINT('Ctrl Pts',(-28.1963676792964,23.8433655921035,-22.1100254359522));
#72023=CARTESIAN_POINT('Ctrl Pts',(-26.3082756674204,19.7998379394444,-21.9111385245773));
#72024=CARTESIAN_POINT('Ctrl Pts',(-21.8857942356115,19.2026233143433,-21.7122516132024));
#72025=CARTESIAN_POINT('Ctrl Pts',(-18.9928088551114,22.6005113218181,-21.5133647018276));
#72026=CARTESIAN_POINT('Ctrl Pts',(-20.2877278058888,26.8711309763936,-21.3144777904526));
#72027=CARTESIAN_POINT('Ctrl Pts',(-24.5806303632008,28.0901449043502,-21.1155908790778));
#72028=CARTESIAN_POINT('Ctrl Pts',(-27.9267030549918,25.137382661233,-20.9167039677029));
#72029=CARTESIAN_POINT('Ctrl Pts',(-27.2511887776856,20.7261823955133,-20.717817056328));
#72030=CARTESIAN_POINT('Ctrl Pts',(-23.174827877961,18.9100631432824,-20.5189301449531));
#72031=CARTESIAN_POINT('Ctrl Pts',(-19.4434504042556,21.3578845158201,-20.3200432335782));
#72032=CARTESIAN_POINT('Ctrl Pts',(-19.4858758862669,25.820306212792,-20.1211563222033));
#72033=CARTESIAN_POINT('Ctrl Pts',(-23.2631189031139,28.1967410456474,-19.9222694108284));
#72034=CARTESIAN_POINT('Ctrl Pts',(-27.3042133797093,26.3034468914392,-19.7233824994535));
#72035=CARTESIAN_POINT('Ctrl Pts',(-27.8957361203712,21.880200553012,-19.5244955880786));
#72036=CARTESIAN_POINT('Ctrl Pts',(-24.4941278792892,18.9915903859367,-19.3256086767037));
#72037=CARTESIAN_POINT('Ctrl Pts',(-20.2251782211997,20.2920042200011,-19.1267217653289));
#72038=CARTESIAN_POINT('Ctrl Pts',(-19.011689934644,24.5864719986112,-18.927834853954));
#72039=CARTESIAN_POINT('Ctrl Pts',(-21.9687558681268,27.9287419440471,-18.7289479425791));
#72040=CARTESIAN_POINT('Ctrl Pts',(-26.3790831466232,27.2475513542133,-18.5300610312042));
#72041=CARTESIAN_POINT('Ctrl Pts',(-28.1899549352836,23.1688566257294,-18.3311741198293));
#72042=CARTESIAN_POINT('Ctrl Pts',(-25.7373335969374,19.4406323977869,-18.1322872084544));
#72043=CARTESIAN_POINT('Ctrl Pts',(-21.2749701935273,19.4888006345782,-17.9334002970795));
#72044=CARTESIAN_POINT('Ctrl Pts',(-18.9033983467632,23.2690988104849,-17.7345133857046));
#72045=CARTESIAN_POINT('Ctrl Pts',(-20.8018915076875,27.3077534182785,-17.5356264743297));
#72046=CARTESIAN_POINT('Ctrl Pts',(-25.2258954270864,27.8935832948393,-17.3367395629548));
#72047=CARTESIAN_POINT('Ctrl Pts',(-28.1101255967088,24.4882604537905,-17.1378526515799));
#72048=CARTESIAN_POINT('Ctrl Pts',(-26.804219033063,20.2209878622919,-16.9389657402051));
#72049=CARTESIAN_POINT('Ctrl Pts',(-22.5081931455219,19.0130272268794,-16.7400788288302));
#72050=CARTESIAN_POINT('Ctrl Pts',(-19.1697314818073,21.9743919533248,-16.5411919174553));
#72051=CARTESIAN_POINT('Ctrl Pts',(-19.8565972560014,26.3838389403481,-16.3423050060804));
#72052=CARTESIAN_POINT('Ctrl Pts',(-23.9376190582342,28.189460266327,-16.1434180947055));
#72053=CARTESIAN_POINT('Ctrl Pts',(-27.662683865842,25.7320430241293,-15.9445311833306));
#72054=CARTESIAN_POINT('Ctrl Pts',(-27.6087729540455,21.2697453047119,-15.7456442719557));
#72055=CARTESIAN_POINT('Ctrl Pts',(-23.8254258798941,18.9030403717642,-15.5467573605808));
#72056=CARTESIAN_POINT('Ctrl Pts',(-19.7892178295995,20.8067293951777,-15.3478704492059));
#72057=CARTESIAN_POINT('Ctrl Pts',(-19.2090817873736,25.2314835686476,-15.148983537831));
#72058=CARTESIAN_POINT('Ctrl Pts',(-22.6181135885969,28.1113289640424,-14.9500966264561));
#72059=CARTESIAN_POINT('Ctrl Pts',(-26.8837020461773,26.7999318336181,-14.7512097150813));
#72060=CARTESIAN_POINT('Ctrl Pts',(-28.0861330298587,22.5023549520939,-14.5523228037064));
#72061=CARTESIAN_POINT('Ctrl Pts',(-25.1204744149729,19.1677070991591,-14.3534358923315));
#72062=CARTESIAN_POINT('Ctrl Pts',(-20.711915022215,19.8602469201477,-14.1545489809566));
#72063=CARTESIAN_POINT('Ctrl Pts',(-18.9115471493331,23.9435890372648,-13.9556620695817));
#72064=CARTESIAN_POINT('Ctrl Pts',(-21.3737562254823,27.6654882551987,-13.7567751582068));
#72065=CARTESIAN_POINT('Ctrl Pts',(-25.8359808705851,27.6058347576825,-13.5578882468319));
#72066=CARTESIAN_POINT('Ctrl Pts',(-28.1978149700514,23.819445051151,-13.359001335457));
#72067=CARTESIAN_POINT('Ctrl Pts',(-26.2889332369806,19.7856902430007,-13.1601144240821));
#72068=CARTESIAN_POINT('Ctrl Pts',(-21.8634361375834,19.2112489959131,-12.9612275127073));
#72069=CARTESIAN_POINT('Ctrl Pts',(-18.9879802859286,22.6239841113762,-12.7623406013324));
#72070=CARTESIAN_POINT('Ctrl Pts',(-20.3048658112352,26.8878813705002,-12.5634536899575));
#72071=CARTESIAN_POINT('Ctrl Pts',(-24.6039865692263,28.0847807110209,-12.3645667785826));
#72072=CARTESIAN_POINT('Ctrl Pts',(-27.9348150886385,25.1148331193285,-12.1656798672077));
#72073=CARTESIAN_POINT('Ctrl Pts',(-27.2366023678193,20.7071686221583,-11.9667929558328));
#72074=CARTESIAN_POINT('Ctrl Pts',(-23.150946698525,18.9120571840877,-11.7679060444579));
#72075=CARTESIAN_POINT('Ctrl Pts',(-19.4322192343616,21.3790540163528,-11.569019133083));
#72076=CARTESIAN_POINT('Ctrl Pts',(-19.4976152188011,25.8411981969398,-11.3701322217081));
#72077=CARTESIAN_POINT('Ctrl Pts',(-23.2870412868087,28.1981575513269,-11.1712453103332));
#72078=CARTESIAN_POINT('Ctrl Pts',(-27.3183361722328,26.2840862700306,-10.9723583989584));
#72079=CARTESIAN_POINT('Ctrl Pts',(-27.8870816728095,21.8578535740801,-10.7734714875834));
#72080=CARTESIAN_POINT('Ctrl Pts',(-24.4706488951754,18.9867920284081,-10.5745845762086));
#72081=CARTESIAN_POINT('Ctrl Pts',(-20.2084498962448,20.3091637676113,-10.3756976648337));
#72082=CARTESIAN_POINT('Ctrl Pts',(-19.0170841811534,24.6098212819959,-10.1768107534588));
#72083=CARTESIAN_POINT('Ctrl Pts',(-21.9913158309151,27.9368249514686,-9.97792384208393));
#72084=CARTESIAN_POINT('Ctrl Pts',(-26.3980781326575,27.2329404871772,-9.77903693070902));
#72085=CARTESIAN_POINT('Ctrl Pts',(-28.1879301629076,23.1449780322445,-9.58015001933414));
#72086=CARTESIAN_POINT('Ctrl Pts',(-25.7161496602922,19.4294284806953,-9.38126310795925));
#72087=CARTESIAN_POINT('Ctrl Pts',(-21.2540933342885,19.5005668437512,-9.18237619658437));
#72088=CARTESIAN_POINT('Ctrl Pts',(-18.9020126285053,23.2930229973027,-8.98348928520946));
#72089=CARTESIAN_POINT('Ctrl Pts',(-20.8212702880001,27.321851283492,-8.78460237383459));
#72090=CARTESIAN_POINT('Ctrl Pts',(-25.2482312499118,27.8849000956191,-8.58571546245968));
#72091=CARTESIAN_POINT('Ctrl Pts',(-28.1148937346359,24.4647753140061,-8.38682855108481));
#72092=CARTESIAN_POINT('Ctrl Pts',(-26.7870379716082,20.2042816341936,-8.1879416397099));
#72093=CARTESIAN_POINT('Ctrl Pts',(-22.4848508234485,19.0184515176349,-7.98905472833502));
#72094=CARTESIAN_POINT('Ctrl Pts',(-19.161677513998,21.996962299634,-7.79016781696012));
#72095=CARTESIAN_POINT('Ctrl Pts',(-19.8712325560094,26.4028151076025,-7.59128090558524));
#72096=CARTESIAN_POINT('Ctrl Pts',(-23.9614950262208,28.1874047657335,-7.39239399421034));
#72097=CARTESIAN_POINT('Ctrl Pts',(-27.6738605115759,25.7108446864556,-7.19350708283546));
#72098=CARTESIAN_POINT('Ctrl Pts',(-27.5969798877205,21.2488836049575,-6.99462017146056));
#72099=CARTESIAN_POINT('Ctrl Pts',(-23.801499929576,18.9016854432229,-6.79573326008568));
#72100=CARTESIAN_POINT('Ctrl Pts',(-19.7751449150443,20.8261263022999,-6.59684634871078));
#72101=CARTESIAN_POINT('Ctrl Pts',(-19.2177937238713,25.2538081983746,-6.3979594373359));
#72102=CARTESIAN_POINT('Ctrl Pts',(-22.6416048451565,28.1160668744714,-6.199072525961));
#72103=CARTESIAN_POINT('Ctrl Pts',(-26.9003861497507,26.7827292867736,-6.00018561458611));
#72104=CARTESIAN_POINT('Ctrl Pts',(-28.0806787038404,22.4790196299904,-5.80129870321121));
#72105=CARTESIAN_POINT('Ctrl Pts',(-25.0978937225233,19.1596821843009,-5.60241179183632));
#72106=CARTESIAN_POINT('Ctrl Pts',(-20.6929577051683,19.8749066288887,-5.40352488046145));
#72107=CARTESIAN_POINT('Ctrl Pts',(-18.9136333747395,23.9674623402106,-5.20463796908654));
#72108=CARTESIAN_POINT('Ctrl Pts',(-21.3949689290764,27.6766376110642,-5.00575105771166));
#72109=CARTESIAN_POINT('Ctrl Pts',(-25.8568273763043,27.5940148537369,-4.80686414633676));
#72110=CARTESIAN_POINT('Ctrl Pts',(-28.1991391066322,23.7955173769579,-4.60797723496188));
#72111=CARTESIAN_POINT('Ctrl Pts',(-26.2695182351733,19.771642302411,-4.40909032358698));
#72112=CARTESIAN_POINT('Ctrl Pts',(-21.8411227379283,19.2199896552601,-4.2102034122121));
#72113=CARTESIAN_POINT('Ctrl Pts',(-18.9832726108445,22.6474814458054,-4.01131650083721));
#72114=CARTESIAN_POINT('Ctrl Pts',(-20.3220898149793,26.9045433219168,-3.81242958946232));
#72115=CARTESIAN_POINT('Ctrl Pts',(-24.6273148527125,28.0792963587734,-3.61354267808743));
#72116=CARTESIAN_POINT('Ctrl Pts',(-27.9428109372554,25.0922421181359,-3.41465576671254));
#72117=CARTESIAN_POINT('Ctrl Pts',(-27.2219182746241,20.6882301867157,-3.21576885533764));
#72118=CARTESIAN_POINT('Ctrl Pts',(-23.1270761001584,18.9141741308522,-3.01688194396275));
#72119=CARTESIAN_POINT('Ctrl Pts',(-19.4210971868294,21.4002810507353,-2.81799503258785));
#72120=CARTESIAN_POINT('Ctrl Pts',(-19.5094619407915,25.8620294740987,-2.61910812121298));
#72121=CARTESIAN_POINT('Ctrl Pts',(-23.3109706452488,28.199450893754,-2.42022120983808));
#72122=CARTESIAN_POINT('Ctrl Pts',(-27.3323591155911,26.2646532056929,-2.22133429846319));
#72123=CARTESIAN_POINT('Ctrl Pts',(-27.8783123050894,21.8355514414517,-2.02244738708831));
#72124=CARTESIAN_POINT('Ctrl Pts',(-24.4471455217919,18.9821145964656,-1.82356047571341));
#72125=CARTESIAN_POINT('Ctrl Pts',(-20.1918101245799,20.3264091997288,-1.62467356433851));
#72126=CARTESIAN_POINT('Ctrl Pts',(-19.0225985505471,24.6331424882292,-1.42578665296364));
#72127=CARTESIAN_POINT('Ctrl Pts',(-22.013917103436,27.9447917206012,-1.22689974158873));
#72128=CARTESIAN_POINT('Ctrl Pts',(-26.4169976551308,27.218232033847,-1.02801283021384));
#72129=CARTESIAN_POINT('Ctrl Pts',(-28.1857824982912,23.1211101779908,-0.829125918838952));
#72130=CARTESIAN_POINT('Ctrl Pts',(-25.6949083302767,19.4183337599166,-0.630239007464067));
#72131=CARTESIAN_POINT('Ctrl Pts',(-21.2332773201901,19.5124403641663,-0.431352096089173));
#72132=CARTESIAN_POINT('Ctrl Pts',(-18.9007500823737,23.3169540003584,-0.232465184714285));
#72133=CARTESIAN_POINT('Ctrl Pts',(-20.8407213826837,27.3358492063947,-0.0335782733393948));
#72134=CARTESIAN_POINT('Ctrl Pts',(-25.2705220785774,27.8761020340494,0.165308638035495));
#72135=CARTESIAN_POINT('Ctrl Pts',(-28.1195409156902,24.441265940594,0.364195549410388));
#72136=CARTESIAN_POINT('Ctrl Pts',(-26.7697711396785,20.1876640698386,0.563082460785278));
#72137=CARTESIAN_POINT('Ctrl Pts',(-22.461536733092,19.0239958950423,0.761969372160167));
#72138=CARTESIAN_POINT('Ctrl Pts',(-19.1537398375437,22.0195738060519,0.96085628353506));
#72139=CARTESIAN_POINT('Ctrl Pts',(-19.8859653451146,26.4217156857727,1.15974319490995));
#72140=CARTESIAN_POINT('Ctrl Pts',(-23.9853600968326,28.1852263868222,1.35863010628484));
#72141=CARTESIAN_POINT('Ctrl Pts',(-27.6849278872261,25.6895890959863,1.55751701765973));
#72142=CARTESIAN_POINT('Ctrl Pts',(-27.5850795885454,21.2280828883946,1.75640392903463));
#72143=CARTESIAN_POINT('Ctrl Pts',(-23.7775673215383,18.9004536954778,1.95529084040951));
#72144=CARTESIAN_POINT('Ctrl Pts',(-19.7611720357803,20.8455953951155,2.15417775178442));
#72145=CARTESIAN_POINT('Ctrl Pts',(-19.2266204647196,25.27608768616,2.35306466315927));
#72146=CARTESIAN_POINT('Ctrl Pts',(-22.6651201796618,28.1206837969411,2.5519515745342));
#72147=CARTESIAN_POINT('Ctrl Pts',(-26.9169814792741,26.7654410836283,2.75083848590907));
#72148=CARTESIAN_POINT('Ctrl Pts',(-28.075104327602,22.4557126941228,2.94972539728396));
#72149=CARTESIAN_POINT('Ctrl Pts',(-25.0752720196569,19.151773613671,3.14861230865887));
#72150=CARTESIAN_POINT('Ctrl Pts',(-20.6740761026041,19.8896637293692,3.34749922003375));
#72151=CARTESIAN_POINT('Ctrl Pts',(-18.9158424643382,23.9913245876556,3.54638613140863));
#72152=CARTESIAN_POINT('Ctrl Pts',(-21.4162387447966,27.6876776232568,3.74527304278354));
#72153=CARTESIAN_POINT('Ctrl Pts',(-25.8776127608824,27.5820877955107,3.94415995415842));
#72154=CARTESIAN_POINT('Ctrl Pts',(-28.2003400539506,23.7715832035748,4.1430468655333));
#72155=CARTESIAN_POINT('Ctrl Pts',(-26.2500311764703,19.7576944899272,4.3419337769082));
#72156=CARTESIAN_POINT('Ctrl Pts',(-21.8188546279217,19.2288450607684,4.54082068828309));
#72157=CARTESIAN_POINT('Ctrl Pts',(-18.978685954606,22.6710027024584,4.73970759965797));
#72158=CARTESIAN_POINT('Ctrl Pts',(-20.3393993607078,26.9211163891241,4.93859451103288));
#72159=CARTESIAN_POINT('Ctrl Pts',(-24.6506145954909,28.0736919929358,5.13748142240776));
#72160=CARTESIAN_POINT('Ctrl Pts',(-27.9506903889628,25.0696102562865,5.33636833378264));
#72161=CARTESIAN_POINT('Ctrl Pts',(-27.2071368872086,20.6693675910284,5.53525524515755));
#72162=CARTESIAN_POINT('Ctrl Pts',(-23.1032167153998,18.9164139274794,5.73414215653244));
#72163=CARTESIAN_POINT('Ctrl Pts',(-19.4100845563787,21.42156505648,5.93302906790731));
#72164=CARTESIAN_POINT('Ctrl Pts',(-19.5214157383157,25.8827994922676,6.13191597928223));
#72165=CARTESIAN_POINT('Ctrl Pts',(-23.3349063443381,28.2006210386571,6.3308028906571));
#72166=CARTESIAN_POINT('Ctrl Pts',(-27.346281838195,26.2451482133761,6.52968980203199));
#72167=CARTESIAN_POINT('Ctrl Pts',(-27.8694282495872,21.8132947461036,6.72857671340688));
#72168=CARTESIAN_POINT('Ctrl Pts',(-24.4236183819465,18.9775582140545,6.92746362478179));
#72169=CARTESIAN_POINT('Ctrl Pts',(-20.1752593471366,20.3437400593731,7.12635053615665));
#72170=CARTESIAN_POINT('Ctrl Pts',(-19.0282328967019,24.6564349993302,7.32523744753157));
#72171=CARTESIAN_POINT('Ctrl Pts',(-22.0365590867865,27.9526420403365,7.52412435890644));
#72172=CARTESIAN_POINT('Ctrl Pts',(-26.4358412127014,27.2034263839771,7.72301127028133));
#72173=CARTESIAN_POINT('Ctrl Pts',(-28.1835119983449,23.0972536954341,7.92189818165623));
#72174=CARTESIAN_POINT('Ctrl Pts',(-25.6736101697574,19.4073485294465,8.12078509303112));
#72175=CARTESIAN_POINT('Ctrl Pts',(-21.212522702829,19.5244208811907,8.31967200440601));
#72176=CARTESIAN_POINT('Ctrl Pts',(-18.8996107418241,23.3408911855124,8.5185589157809));
#72177=CARTESIAN_POINT('Ctrl Pts',(-20.8602442763108,27.3497468160602,8.71744582715579));
#72178=CARTESIAN_POINT('Ctrl Pts',(-25.2927673224061,27.8671893432668,8.91633273853067));
#72179=CARTESIAN_POINT('Ctrl Pts',(-28.1240670167278,24.417732956521,9.11521964990558));
#72180=CARTESIAN_POINT('Ctrl Pts',(-26.7524189948213,20.1711356095702,9.31410656128044));
#72181=CARTESIAN_POINT('Ctrl Pts',(-22.4382514922448,19.0296602121829,9.51299347265536));
#72182=CARTESIAN_POINT('Ctrl Pts',(-19.1459186627819,22.0422258734042,9.71188038403022));
#72183=CARTESIAN_POINT('Ctrl Pts',(-19.9007952329182,26.4405401740185,9.91076729540515));
#72184=CARTESIAN_POINT('Ctrl Pts',(-24.0092136376771,28.182925187317,10.10965420678));
#72185=CARTESIAN_POINT('Ctrl Pts',(-27.6958856995223,25.668276815966,10.308541118155));
#72186=CARTESIAN_POINT('Ctrl Pts',(-27.5730723718623,21.2073437062143,10.5074280295298));
#72187=CARTESIAN_POINT('Ctrl Pts',(-23.7536286899636,18.8993451611687,10.7063149409047));
#72188=CARTESIAN_POINT('Ctrl Pts',(-19.74729956207,20.8651361577193,10.9052018522796));
#72189=CARTESIAN_POINT('Ctrl Pts',(-19.2355617760216,25.2983214416274,11.1040887636545));
#72190=CARTESIAN_POINT('Ctrl Pts',(-22.6886589689878,28.125179609109,11.3029756750294));
#72191=CARTESIAN_POINT('Ctrl Pts',(-26.9334875949936,26.7480676822966,11.5018625864043));
#72192=CARTESIAN_POINT('Ctrl Pts',(-28.0694100488568,22.4324347620937,11.7007494977791));
#72193=CARTESIAN_POINT('Ctrl Pts',(-25.0526099058185,19.143981596836,11.8996364091541));
#72194=CARTESIAN_POINT('Ctrl Pts',(-20.6552707148596,19.9045178305457,12.098523320529));
#72195=CARTESIAN_POINT('Ctrl Pts',(-18.9181743595909,24.0151751472824,12.2974102319038));
#72196=CARTESIAN_POINT('Ctrl Pts',(-21.4375651090214,27.6986079992308,12.4962971432787));
#72197=CARTESIAN_POINT('Ctrl Pts',(-25.8983364735341,27.5700538990548,12.6951840546536));
#72198=CARTESIAN_POINT('Ctrl Pts',(-28.2014177801836,23.747643165226,12.8940709660285));
#72199=CARTESIAN_POINT('Ctrl Pts',(-26.2304725772522,19.7438471751471,13.0929578774034));
#72200=CARTESIAN_POINT('Ctrl Pts',(-21.7966323976384,19.2378149777817,13.2918447887783));
#72201=CARTESIAN_POINT('Ctrl Pts',(-18.9742204387534,22.6945472580531,13.4907317001532));
#72202=CARTESIAN_POINT('Ctrl Pts',(-20.3567939897411,26.937600132958,13.6896186115281));
#72203=CARTESIAN_POINT('Ctrl Pts',(-24.6738851801498,28.0679677620165,13.888505522903));
#72204=CARTESIAN_POINT('Ctrl Pts',(-27.958453234966,25.0469381334941,14.0873924342778));
#72205=CARTESIAN_POINT('Ctrl Pts',(-27.19225859726,20.6505813349302,14.2862793456527));
#72206=CARTESIAN_POINT('Ctrl Pts',(-23.0793691764913,18.9187765146178,14.4851662570276));
#72207=CARTESIAN_POINT('Ctrl Pts',(-19.3991816348293,21.4429054695892,14.6840531684025));
#72208=CARTESIAN_POINT('Ctrl Pts',(-19.533476294614,25.9035077010689,14.8829400797774));
#72209=CARTESIAN_POINT('Ctrl Pts',(-23.3588477498126,28.2016679550287,15.0818269911523));
#72210=CARTESIAN_POINT('Ctrl Pts',(-27.360103971111,26.2255718099364,15.2807139025272));
#72211=CARTESIAN_POINT('Ctrl Pts',(-27.8604297417186,21.7910840778083,15.4796008139021));
#72212=CARTESIAN_POINT('Ctrl Pts',(-24.4000680990767,18.9731230019129,15.678487725277));
#72213=CARTESIAN_POINT('Ctrl Pts',(-20.1587980024883,20.3611558872995,15.8773746366519));
#72214=CARTESIAN_POINT('Ctrl Pts',(-19.0339870703151,24.6796981980787,16.0762615480267));
#72215=CARTESIAN_POINT('Ctrl Pts',(-22.0592411809838,27.9603757026515,16.2751484594016));
#72216=CARTESIAN_POINT('Ctrl Pts',(-26.4546083060402,27.1885239298975,16.4740353707766));
#72217=CARTESIAN_POINT('Ctrl Pts',(-28.1811187232336,23.0734092167393,16.6729222821514));
#72218=CARTESIAN_POINT('Ctrl Pts',(-25.6522557431073,19.3964730803787,16.8718091935263));
#72219=CARTESIAN_POINT('Ctrl Pts',(-21.1918300321744,19.5365080773572,17.0706961049012));
#72220=CARTESIAN_POINT('Ctrl Pts',(-18.8985946370477,23.3648339184615,17.2695830162761));
#72221=CARTESIAN_POINT('Ctrl Pts',(-20.8798384515504,27.3635437442206,17.468469927651));
#72222=CARTESIAN_POINT('Ctrl Pts',(-25.3149663919288,27.8581622594458,17.6673568390259));
#72223=CARTESIAN_POINT('Ctrl Pts',(-28.1284719178129,24.3941769853794,17.8662437504008));
#72224=CARTESIAN_POINT('Ctrl Pts',(-26.7349819968456,20.1546966913704,18.0651306617757));
#72225=CARTESIAN_POINT('Ctrl Pts',(-22.4149957179343,19.0354443189599,18.2640175731505));
#72226=CARTESIAN_POINT('Ctrl Pts',(-19.1382141969635,22.0649179014414,18.4629044845255));
#72227=CARTESIAN_POINT('Ctrl Pts',(-19.915721826448,26.4592880735162,18.6617913959003));
#72228=CARTESIAN_POINT('Ctrl Pts',(-24.0330550166675,28.1805012281969,18.8606783072753));
#72229=CARTESIAN_POINT('Ctrl Pts',(-27.7067336580968,25.6469084111413,19.0595652186501));
#72230=CARTESIAN_POINT('Ctrl Pts',(-27.560958555846,21.1866666079772,19.258452130025));
#72231=CARTESIAN_POINT('Ctrl Pts',(-23.7296846691934,18.8983598696701,19.4573390413999));
#72232=CARTESIAN_POINT('Ctrl Pts',(-19.7335278615154,20.8847480723076,19.6562259527748));
#72233=CARTESIAN_POINT('Ctrl Pts',(-19.2446174208448,25.320508875612,19.8551128641497));
#72234=CARTESIAN_POINT('Ctrl Pts',(-22.7122205893882,28.1295541918424,20.0539997755246));
#72235=CARTESIAN_POINT('Ctrl Pts',(-26.9499040595195,26.73060954315,20.2528866868994));
#72236=CARTESIAN_POINT('Ctrl Pts',(-28.0635960184952,22.4091864507369,20.4517735982743));
#72237=CARTESIAN_POINT('Ctrl Pts',(-25.0299079815236,19.1363063402742,20.6506605096492));
#72238=CARTESIAN_POINT('Ctrl Pts',(-20.6365420402524,19.9194685388046,20.8495474210241));
#72239=CARTESIAN_POINT('Ctrl Pts',(-18.9206289987058,24.0390133870832,21.048434332399));
#72240=CARTESIAN_POINT('Ctrl Pts',(-21.4589474566307,27.709428449346,21.2473212437739));
#72241=CARTESIAN_POINT('Ctrl Pts',(-25.9189979651091,27.5579134832514,21.4462081551488));
#72242=CARTESIAN_POINT('Ctrl Pts',(-28.2023722567724,23.7236978962898,21.6450950665237));
#72243=CARTESIAN_POINT('Ctrl Pts',(-26.2108429557959,19.7301007250066,21.8439819778986));
#72244=CARTESIAN_POINT('Ctrl Pts',(-21.7744566359379,19.246899168609,22.0428688892735));
#72245=CARTESIAN_POINT('Ctrl Pts',(-18.969876181617,22.7181144886908,22.2417558006483));
#72246=CARTESIAN_POINT('Ctrl Pts',(-20.3742732411446,26.9539941166208,22.4406427120233));
#72247=CARTESIAN_POINT('Ctrl Pts',(-24.69712599005,28.0621238177003,22.6395296233981));
#72248=CARTESIAN_POINT('Ctrl Pts',(-27.9660992695595,25.0242263505381,22.838416534773));
#72249=CARTESIAN_POINT('Ctrl Pts',(-27.1772837990336,20.6318719162339,23.0373034461479));
#72250=CARTESIAN_POINT('Ctrl Pts',(-23.0555341153588,18.9212618296573,23.2361903575228));
#72251=CARTESIAN_POINT('Ctrl Pts',(-19.3883887110968,21.4643017245793,23.4350772688977));
#72252=CARTESIAN_POINT('Ctrl Pts',(-19.5456432900926,25.9241535517461,23.6339641802726));
#72253=CARTESIAN_POINT('Ctrl Pts',(-23.3827942272672,28.2025916151584,23.8328510916475));
#72254=CARTESIAN_POINT('Ctrl Pts',(-27.3738251480522,26.2059245140626,24.0317380030224));
#72255=CARTESIAN_POINT('Ctrl Pts',(-27.8513170199678,21.7689200252309,24.2306249143973));
#72256=CARTESIAN_POINT('Ctrl Pts',(-24.3764952971655,18.9688090773561,24.4295118257721));
#72257=CARTESIAN_POINT('Ctrl Pts',(-20.142426526967,20.378656222412,24.6283987371471));
#72258=CARTESIAN_POINT('Ctrl Pts',(-19.0398609186662,24.7029314672756,24.8272856485219));
#72259=CARTESIAN_POINT('Ctrl Pts',(-22.0819627854415,27.9679925040413,25.0261725598969));
#72260=CARTESIAN_POINT('Ctrl Pts',(-26.4732984369799,27.1735250638085,25.2250594712717));
#72261=CARTESIAN_POINT('Ctrl Pts',(-28.1786027380087,23.0495773788407,25.4239463826466));
#72262=CARTESIAN_POINT('Ctrl Pts',(-25.6308456131075,19.3857076912915,25.6228332940215));
#72263=CARTESIAN_POINT('Ctrl Pts',(-21.1711998623744,19.5487016505103,25.8217202053964));
#72264=CARTESIAN_POINT('Ctrl Pts',(-18.8977017839806,23.3887815305051,26.0206071167713));
#72265=CARTESIAN_POINT('Ctrl Pts',(-20.8995034099329,27.3772396899469,26.2194940281462));
#72266=CARTESIAN_POINT('Ctrl Pts',(-25.3371186597208,27.8490208996796,26.4183809395211));
#72267=CARTESIAN_POINT('Ctrl Pts',(-28.1327555762001,24.3705988819437,26.6172678508959));
#72268=CARTESIAN_POINT('Ctrl Pts',(-26.7174604681214,20.1383473154802,26.8161547622709));
#72269=CARTESIAN_POINT('Ctrl Pts',(-22.3917702901644,19.0413488841658,27.0150416736457));
#72270=CARTESIAN_POINT('Ctrl Pts',(-19.1306261462195,22.0876477366323,27.2139285850206));
#72271=CARTESIAN_POINT('Ctrl Pts',(-19.9307456705459,26.4779618183849,27.4128154963955));
#72272=CARTESIAN_POINT('Ctrl Pts',(-24.0568818264179,28.1779490395339,27.6117024077704));
#72273=CARTESIAN_POINT('Ctrl Pts',(-27.7174748282288,25.625494897365,27.8105893191453));
#72274=CARTESIAN_POINT('Ctrl Pts',(-27.54873213085,21.1660324105898,28.0094762305202));
#72275=CARTESIAN_POINT('Ctrl Pts',(-23.7057478472643,18.8975351032718,28.2083631418951));
#72276=CARTESIAN_POINT('Ctrl Pts',(-19.7198347282729,20.904360271747,28.40725005327));
#72277=CARTESIAN_POINT('Ctrl Pts',(-19.2538297777398,25.3427822320754,28.6061369646448));
#72278=CARTESIAN_POINT('Ctrl Pts',(-22.7357239416392,28.1335566023601,28.8050238760198));
#72279=CARTESIAN_POINT('Ctrl Pts',(-26.9663824108126,26.7135408490309,29.0039107873946));
#72280=CARTESIAN_POINT('Ctrl Pts',(-28.0573752707713,22.3850730121439,29.2027976987696));
#72281=CARTESIAN_POINT('Ctrl Pts',(-25.0077103293766,19.1304459024294,29.4016846101444));
#72282=CARTESIAN_POINT('Ctrl Pts',(-20.6168533946832,19.9312505216016,29.6005715215193));
#72283=CARTESIAN_POINT('Ctrl Pts',(-18.9252562888303,24.0694825381366,29.7994584328942));
#72284=CARTESIAN_POINT('Ctrl Pts',(-20.6254760904471,26.4925251454433,29.9320497071441));
#72285=CARTESIAN_POINT('Ctrl Pts',(-21.8002837957285,27.0756816094313,29.9983453442691));
#72286=CARTESIAN_POINT('Ctrl Pts',(-21.4056980533955,20.5397621095878,-75.2735003480446));
#72287=CARTESIAN_POINT('Ctrl Pts',(-20.4017695023793,21.2548416367245,-75.2071605181002));
#72288=CARTESIAN_POINT('Ctrl Pts',(-19.1839163191839,23.7551997076661,-75.0745250510308));
#72289=CARTESIAN_POINT('Ctrl Pts',(-21.3678897177328,27.3419747835828,-74.8755939468365));
#72290=CARTESIAN_POINT('Ctrl Pts',(-25.5584650129784,27.4321216345841,-74.6767070354616));
#72291=CARTESIAN_POINT('Ctrl Pts',(-27.9027813811771,23.9610038383834,-74.4778201240867));
#72292=CARTESIAN_POINT('Ctrl Pts',(-26.2479589884383,20.1093797044535,-74.2789332127118));
#72293=CARTESIAN_POINT('Ctrl Pts',(-22.1139262816015,19.4212427346286,-74.080046301337));
#72294=CARTESIAN_POINT('Ctrl Pts',(-19.2998863162224,22.526459948928,-73.881159389962));
#72295=CARTESIAN_POINT('Ctrl Pts',(-20.3915033145888,26.5729088825349,-73.6822724785872));
#72296=CARTESIAN_POINT('Ctrl Pts',(-24.3857796829293,27.8415529321505,-73.4833855672123));
#72297=CARTESIAN_POINT('Ctrl Pts',(-27.6122580265173,25.1669828476232,-73.2844986558374));
#72298=CARTESIAN_POINT('Ctrl Pts',(-27.1061080032505,21.0067073707803,-73.0856117444625));
#72299=CARTESIAN_POINT('Ctrl Pts',(-23.3324228432654,19.1837698863755,-72.8867248330876));
#72300=CARTESIAN_POINT('Ctrl Pts',(-19.7589075818257,21.3732408577498,-72.6878379217128));
#72301=CARTESIAN_POINT('Ctrl Pts',(-19.6693153490062,25.5632109755048,-72.4889510103378));
#72302=CARTESIAN_POINT('Ctrl Pts',(-23.1459761467135,27.9034376590548,-72.290064098963));
#72303=CARTESIAN_POINT('Ctrl Pts',(-26.9941322368646,26.2434591040856,-72.091177187588));
#72304=CARTESIAN_POINT('Ctrl Pts',(-27.6776550976768,22.1086505701856,-71.8922902762132));
#72305=CARTESIAN_POINT('Ctrl Pts',(-24.5684448262307,19.2985527977709,-71.6934033648382));
#72306=CARTESIAN_POINT('Ctrl Pts',(-20.5236022282072,20.3954061795816,-71.4945164534635));
#72307=CARTESIAN_POINT('Ctrl Pts',(-19.2599946077614,24.3912960927353,-71.2956295420884));
#72308=CARTESIAN_POINT('Ctrl Pts',(-21.938770283371,27.6143381651901,-71.0967426307136));
#72309=CARTESIAN_POINT('Ctrl Pts',(-26.0983615045746,27.1028301799775,-70.8978557193387));
#72310=CARTESIAN_POINT('Ctrl Pts',(-27.9164566287204,23.3268045121349,-70.6989688079639));
#72311=CARTESIAN_POINT('Ctrl Pts',(-25.7223803781076,19.7561086463548,-70.5000818965888));
#72312=CARTESIAN_POINT('Ctrl Pts',(-21.5323028041158,19.6719093116581,-70.3011949852142));
#72313=CARTESIAN_POINT('Ctrl Pts',(-19.1965499351028,23.1515785717638,-70.102308073839));
#72314=CARTESIAN_POINT('Ctrl Pts',(-20.8614806196438,26.99759539649,-69.9034211624643));
#72315=CARTESIAN_POINT('Ctrl Pts',(-24.9971647208865,27.6757964163086,-69.7045342510893));
#72316=CARTESIAN_POINT('Ctrl Pts',(-27.803259198295,24.5629723938821,-69.5056473397145));
#72317=CARTESIAN_POINT('Ctrl Pts',(-26.701201144539,20.5195446829723,-69.3067604283396));
#72318=CARTESIAN_POINT('Ctrl Pts',(-22.7036884719959,19.2610805231846,-69.1078735169647));
#72319=CARTESIAN_POINT('Ctrl Pts',(-19.4840963935033,21.9440017775089,-68.9089866055898));
#72320=CARTESIAN_POINT('Ctrl Pts',(-20.0009570528289,26.1029312872671,-68.7100996942149));
#72321=CARTESIAN_POINT('Ctrl Pts',(-23.7793193265963,27.916165452151,-68.5112127828401));
#72322=CARTESIAN_POINT('Ctrl Pts',(-27.3471886375126,25.7174958114912,-68.3123258714651));
#72323=CARTESIAN_POINT('Ctrl Pts',(-27.4259955942737,21.5273133486342,-68.1134389600903));
#72324=CARTESIAN_POINT('Ctrl Pts',(-23.9433232853466,19.1960404780467,-67.9145520487153));
#72325=CARTESIAN_POINT('Ctrl Pts',(-20.0994522807164,20.8659193084615,-67.7156651373405));
#72326=CARTESIAN_POINT('Ctrl Pts',(-19.4265741271225,25.0024727771007,-67.5167782259656));
#72327=CARTESIAN_POINT('Ctrl Pts',(-22.5430067970579,27.804558968184,-67.3178913145907));
#72328=CARTESIAN_POINT('Ctrl Pts',(-26.585012896769,26.6972982498353,-67.1190044032158));
#72329=CARTESIAN_POINT('Ctrl Pts',(-27.8383315262235,22.6981693419905,-66.9201174918409));
#72330=CARTESIAN_POINT('Ctrl Pts',(-25.1512691288489,19.4820326407425,-66.721230580466));
#72331=CARTESIAN_POINT('Ctrl Pts',(-20.9930082225112,20.0042450911138,-66.5223436690911));
#72332=CARTESIAN_POINT('Ctrl Pts',(-19.1846380177503,23.7849377275274,-66.3234567577163));
#72333=CARTESIAN_POINT('Ctrl Pts',(-21.3878974082326,27.3499745669935,-66.1245698463413));
#72334=CARTESIAN_POINT('Ctrl Pts',(-25.5781778196954,27.4233890193208,-65.9256829349665));
#72335=CARTESIAN_POINT('Ctrl Pts',(-27.9049668311952,23.9377194273396,-65.7267960235915));
#72336=CARTESIAN_POINT('Ctrl Pts',(-26.2301426203391,20.0960006100355,-65.5279091122166));
#72337=CARTESIAN_POINT('Ctrl Pts',(-22.0927266352278,19.4284464364696,-65.3290222008418));
#72338=CARTESIAN_POINT('Ctrl Pts',(-19.2946533711521,22.5484825928889,-65.1301352894669));
#72339=CARTESIAN_POINT('Ctrl Pts',(-20.4071149203071,26.589060386986,-64.931248378092));
#72340=CARTESIAN_POINT('Ctrl Pts',(-24.4078534402043,27.8372314104878,-64.7323614667171));
#72341=CARTESIAN_POINT('Ctrl Pts',(-27.6205294377469,25.146032320247,-64.5334745553423));
#72342=CARTESIAN_POINT('Ctrl Pts',(-27.0929660611986,20.9884469041403,-64.3345876439672));
#72343=CARTESIAN_POINT('Ctrl Pts',(-23.3099493236091,19.1849436544572,-64.1357007325925));
#72344=CARTESIAN_POINT('Ctrl Pts',(-19.7477508598977,21.3927891457973,-63.9368138212175));
#72345=CARTESIAN_POINT('Ctrl Pts',(-19.6797290335917,25.583160566047,-63.7379269098427));
#72346=CARTESIAN_POINT('Ctrl Pts',(-23.1683901357664,27.9054618649038,-63.5390399984677));
#72347=CARTESIAN_POINT('Ctrl Pts',(-27.0079504032068,26.2256950473984,-63.3401530870929));
#72348=CARTESIAN_POINT('Ctrl Pts',(-27.6701794911614,22.0874233980783,-63.1412661757179));
#72349=CARTESIAN_POINT('Ctrl Pts',(-24.5465450155675,19.2933676950938,-62.9423792643431));
#72350=CARTESIAN_POINT('Ctrl Pts',(-20.5074022189665,20.4110282326302,-62.7434923529682));
#72351=CARTESIAN_POINT('Ctrl Pts',(-19.2643808686007,24.4133697386781,-62.5446054415934));
#72352=CARTESIAN_POINT('Ctrl Pts',(-21.9597121946251,27.6225797117789,-62.3457185302184));
#72353=CARTESIAN_POINT('Ctrl Pts',(-26.1166152348344,27.0896662827878,-62.1468316188435));
#72354=CARTESIAN_POINT('Ctrl Pts',(-27.9152485425322,23.3043317093402,-61.9479447074687));
#72355=CARTESIAN_POINT('Ctrl Pts',(-25.7028206069009,19.7449775209885,-61.7490577960937));
#72356=CARTESIAN_POINT('Ctrl Pts',(-21.5123651178303,19.6823484333594,-61.5501708847189));
#72357=CARTESIAN_POINT('Ctrl Pts',(-19.1945553777414,23.173995267913,-61.3512839733439));
#72358=CARTESIAN_POINT('Ctrl Pts',(-20.8792620199174,27.0113906265264,-61.1523970619691));
#72359=CARTESIAN_POINT('Ctrl Pts',(-25.0183824797664,27.6682935321061,-60.9535101505941));
#72360=CARTESIAN_POINT('Ctrl Pts',(-27.8084159942293,24.5410659106062,-60.7546232392194));
#72361=CARTESIAN_POINT('Ctrl Pts',(-26.685558319347,20.5033648010071,-60.5557363278443));
#72362=CARTESIAN_POINT('Ctrl Pts',(-22.681620455705,19.2654951824313,-60.3568494164696));
#72363=CARTESIAN_POINT('Ctrl Pts',(-19.4758818220422,21.9649542803137,-60.1579625050946));
#72364=CARTESIAN_POINT('Ctrl Pts',(-20.0141444208808,26.1211680600887,-59.9590755937197));
#72365=CARTESIAN_POINT('Ctrl Pts',(-23.8017905610305,27.9149284469595,-59.7601886823449));
#72366=CARTESIAN_POINT('Ctrl Pts',(-27.358294579128,25.6979217311929,-59.5613017709699));
#72367=CARTESIAN_POINT('Ctrl Pts',(-27.4155308243559,21.5073891134064,-59.3624148595951));
#72368=CARTESIAN_POINT('Ctrl Pts',(-23.9209040401828,19.1940747707718,-59.1635279482201));
#72369=CARTESIAN_POINT('Ctrl Pts',(-20.0856799457743,20.8837184474582,-58.9646410368453));
#72370=CARTESIAN_POINT('Ctrl Pts',(-19.434104310512,25.0236808627504,-58.7657541254704));
#72371=CARTESIAN_POINT('Ctrl Pts',(-22.5649198986986,27.809687567923,-58.5668672140955));
#72372=CARTESIAN_POINT('Ctrl Pts',(-26.6011726341775,26.6816346153375,-58.3679803027206));
#72373=CARTESIAN_POINT('Ctrl Pts',(-27.8338884708415,22.6761070253018,-58.1690933913457));
#72374=CARTESIAN_POINT('Ctrl Pts',(-25.1303060718632,19.473845040324,-57.9702064799708));
#72375=CARTESIAN_POINT('Ctrl Pts',(-20.9747884359177,20.0174559175559,-57.7713195685959));
#72376=CARTESIAN_POINT('Ctrl Pts',(-19.1859039406453,23.8074073514233,-57.5724326572211));
#72377=CARTESIAN_POINT('Ctrl Pts',(-21.407485764808,27.3610553090927,-57.3735457458461));
#72378=CARTESIAN_POINT('Ctrl Pts',(-25.5980885710774,27.4128986171263,-57.1746588344714));
#72379=CARTESIAN_POINT('Ctrl Pts',(-27.9069036850169,23.9152976710286,-56.9757719230963));
#72380=CARTESIAN_POINT('Ctrl Pts',(-26.2123257721566,20.0822511926065,-56.7768850117216));
#72381=CARTESIAN_POINT('Ctrl Pts',(-22.0715282579012,19.4360039067815,-56.5779981003465));
#72382=CARTESIAN_POINT('Ctrl Pts',(-19.2895529761186,22.5704022764929,-56.3791111889718));
#72383=CARTESIAN_POINT('Ctrl Pts',(-20.4227993381602,26.6051999531328,-56.1802242775967));
#72384=CARTESIAN_POINT('Ctrl Pts',(-24.4299100207564,27.8327599662979,-55.981337366222));
#72385=CARTESIAN_POINT('Ctrl Pts',(-27.6286900535603,25.1250587438152,-55.782450454847));
#72386=CARTESIAN_POINT('Ctrl Pts',(-27.0797317982467,20.9702441339412,-55.5835635434722));
#72387=CARTESIAN_POINT('Ctrl Pts',(-23.2874813474644,19.1862384929635,-55.3846766320972));
#72388=CARTESIAN_POINT('Ctrl Pts',(-19.7366953356669,21.4123917462059,-55.1857897207224));
#72389=CARTESIAN_POINT('Ctrl Pts',(-19.690245050689,25.6030578006088,-54.9869028093475));
#72390=CARTESIAN_POINT('Ctrl Pts',(-23.1908143660906,27.9073698620638,-54.7880158979726));
#72391=CARTESIAN_POINT('Ctrl Pts',(-27.0216768803512,26.2078605195381,-54.5891289865977));
#72392=CARTESIAN_POINT('Ctrl Pts',(-27.6625947464435,22.0662347641827,-54.3902420752228));
#72393=CARTESIAN_POINT('Ctrl Pts',(-24.5246187863028,19.2882955132131,-54.1913551638479));
#72394=CARTESIAN_POINT('Ctrl Pts',(-20.4912828508116,20.4267334078627,-53.9924682524731));
#72395=CARTESIAN_POINT('Ctrl Pts',(-19.2688806941927,24.4354205465643,-53.7935813410981));
#72396=CARTESIAN_POINT('Ctrl Pts',(-21.9806962557675,27.6307133294717,-53.5946944297233));
#72397=CARTESIAN_POINT('Ctrl Pts',(-26.1348009584921,27.0764086052445,-53.3958075183484));
#72398=CARTESIAN_POINT('Ctrl Pts',(-27.9139247905591,23.2818654181574,-53.1969206069734));
#72399=CARTESIAN_POINT('Ctrl Pts',(-25.6832037951245,19.7339472329358,-52.9980336955985));
#72400=CARTESIAN_POINT('Ctrl Pts',(-21.4924814330418,19.692890047943,-52.7991467842237));
#72401=CARTESIAN_POINT('Ctrl Pts',(-19.1926762404031,23.1964219351121,-52.6002598728488));
#72402=CARTESIAN_POINT('Ctrl Pts',(-20.8971141979184,27.0250941406527,-52.4013729614739));
#72403=CARTESIAN_POINT('Ctrl Pts',(-25.0395613351389,27.6606815255441,-52.202486050099));
#72404=CARTESIAN_POINT('Ctrl Pts',(-27.8134599545569,24.5191331719944,-52.0035991387242));
#72405=CARTESIAN_POINT('Ctrl Pts',(-26.6698324127457,20.4872656575404,-51.8047122273491));
#72406=CARTESIAN_POINT('Ctrl Pts',(-22.6595754570046,19.270023381973,-51.6058253159744));
#72407=CARTESIAN_POINT('Ctrl Pts',(-19.4677752159405,21.9859487914132,-51.4069384045994));
#72408=CARTESIAN_POINT('Ctrl Pts',(-20.0274254910585,26.1393367070863,-51.2080514932246));
#72409=CARTESIAN_POINT('Ctrl Pts',(-23.8242551300434,27.9135757837119,-51.0091645818496));
#72410=CARTESIAN_POINT('Ctrl Pts',(-27.3692996127346,25.6782907405373,-50.8102776704749));
#72411=CARTESIAN_POINT('Ctrl Pts',(-27.4049636297446,21.4875190113221,-50.6113907590997));
#72412=CARTESIAN_POINT('Ctrl Pts',(-23.8984749732513,19.1922244963672,-50.4125038477251));
#72413=CARTESIAN_POINT('Ctrl Pts',(-20.0719994173611,20.9015882460338,-50.2136169363501));
#72414=CARTESIAN_POINT('Ctrl Pts',(-19.4417435663115,25.0448499045242,-50.0147300249752));
#72415=CARTESIAN_POINT('Ctrl Pts',(-22.586859110333,27.8147032983438,-49.8158431136003));
#72416=CARTESIAN_POINT('Ctrl Pts',(-26.6172515262933,26.6658880034122,-49.6169562022254));
#72417=CARTESIAN_POINT('Ctrl Pts',(-27.8293319048493,22.6540678722973,-49.4180692908506));
#72418=CARTESIAN_POINT('Ctrl Pts',(-25.1093011455769,19.4657654592394,-49.2191823794755));
#72419=CARTESIAN_POINT('Ctrl Pts',(-20.9566368956703,20.0307603583726,-49.0202954681009));
#72420=CARTESIAN_POINT('Ctrl Pts',(-19.1872855129273,23.829870161061,-48.8214085567257));
#72421=CARTESIAN_POINT('Ctrl Pts',(-21.4271309018305,27.3720350700269,-48.6225216453511));
#72422=CARTESIAN_POINT('Ctrl Pts',(-25.6179450575493,27.4023058599883,-48.423634733976));
#72423=CARTESIAN_POINT('Ctrl Pts',(-27.9087250934233,23.8928662415108,-48.2247478226013));
#72424=CARTESIAN_POINT('Ctrl Pts',(-26.1944383826017,20.0685936725639,-48.0258609112262));
#72425=CARTESIAN_POINT('Ctrl Pts',(-22.0503690647856,19.4436703991666,-47.8269739998515));
#72426=CARTESIAN_POINT('Ctrl Pts',(-19.2845654839116,22.5923479248151,-47.6280870884765));
#72427=CARTESIAN_POINT('Ctrl Pts',(-20.4385666293305,26.621258567268,-47.4292001771016));
#72428=CARTESIAN_POINT('Ctrl Pts',(-24.4519432915644,27.828175041402,-47.2303132657268));
#72429=CARTESIAN_POINT('Ctrl Pts',(-27.6367425962466,25.1040434371298,-47.0314263543518));
#72430=CARTESIAN_POINT('Ctrl Pts',(-27.0664040088257,20.9521097305061,-46.832539442977));
#72431=CARTESIAN_POINT('Ctrl Pts',(-23.2650203344038,19.1876489719916,-46.6336525316021));
#72432=CARTESIAN_POINT('Ctrl Pts',(-19.7257408655894,21.4320509970594,-46.4347656202272));
#72433=CARTESIAN_POINT('Ctrl Pts',(-19.70086335281,25.6229006385828,-46.2358787088523));
#72434=CARTESIAN_POINT('Ctrl Pts',(-23.2132481210444,27.9091624014555,-46.0369917974774));
#72435=CARTESIAN_POINT('Ctrl Pts',(-27.0353113694039,26.1899555686286,-45.8381048861025));
#72436=CARTESIAN_POINT('Ctrl Pts',(-27.6549010301699,22.0450854547685,-45.6392179747276));
#72437=CARTESIAN_POINT('Ctrl Pts',(-24.5026667376387,19.28333626748,-45.4403310633527));
#72438=CARTESIAN_POINT('Ctrl Pts',(-20.4752445412525,20.4425213521647,-45.2414441519778));
#72439=CARTESIAN_POINT('Ctrl Pts',(-19.2734939703991,24.4574478986848,-45.0425572406029));
#72440=CARTESIAN_POINT('Ctrl Pts',(-22.001721908047,27.6387388204235,-44.843670329228));
#72441=CARTESIAN_POINT('Ctrl Pts',(-26.1529181950812,27.0630574892923,-44.6447834178532));
#72442=CARTESIAN_POINT('Ctrl Pts',(-27.9124854071207,23.2594062388733,-44.4458965064782));
#72443=CARTESIAN_POINT('Ctrl Pts',(-25.6635304629989,19.7230180718576,-44.2470095951034));
#72444=CARTESIAN_POINT('Ctrl Pts',(-21.4726522764289,19.7035338774615,-44.0481226837284));
#72445=CARTESIAN_POINT('Ctrl Pts',(-19.1909125729949,23.2188579783477,-43.8492357723537));
#72446=CARTESIAN_POINT('Ctrl Pts',(-20.9150366805287,27.0387055761348,-43.6503488609786));
#72447=CARTESIAN_POINT('Ctrl Pts',(-25.0607007258249,27.6529605981239,-43.4514619496039));
#72448=CARTESIAN_POINT('Ctrl Pts',(-27.8183909456027,24.4971747593445,-43.2525750382288));
#72449=CARTESIAN_POINT('Ctrl Pts',(-26.6540238414595,20.4712476791197,-43.0536881268542));
#72450=CARTESIAN_POINT('Ctrl Pts',(-22.6375540600525,19.2746650018495,-42.854801215479));
#72451=CARTESIAN_POINT('Ctrl Pts',(-19.4597767900149,22.0069847544649,-42.6559143041044));
#72452=CARTESIAN_POINT('Ctrl Pts',(-20.0407999114304,26.1574367468242,-42.4570273927293));
#72453=CARTESIAN_POINT('Ctrl Pts',(-23.8467124383548,27.9121074982472,-42.2581404813545));
#72454=CARTESIAN_POINT('Ctrl Pts',(-27.3802034467131,25.6586033597219,-42.0592535699795));
#72455=CARTESIAN_POINT('Ctrl Pts',(-27.3942942904567,21.4677035689108,-41.8603666586047));
#72456=CARTESIAN_POINT('Ctrl Pts',(-23.8760366788917,19.1904897038634,-41.6614797472298));
#72457=CARTESIAN_POINT('Ctrl Pts',(-20.0584110579928,20.9195282306625,-41.4625928358549));
#72458=CARTESIAN_POINT('Ctrl Pts',(-19.4494916920911,25.0659793414713,-41.26370592448));
#72459=CARTESIAN_POINT('Ctrl Pts',(-22.6088238506017,27.8196060265358,-41.0648190131051));
#72460=CARTESIAN_POINT('Ctrl Pts',(-26.6332491470472,26.6500588313235,-40.8659321017303));
#72461=CARTESIAN_POINT('Ctrl Pts',(-27.8246619489901,22.6320524669849,-40.6670451903554));
#72462=CARTESIAN_POINT('Ctrl Pts',(-25.0882549065923,19.4577941115868,-40.4681582789804));
#72463=CARTESIAN_POINT('Ctrl Pts',(-20.9385540827603,20.0441580610137,-40.2692713676056));
#72464=CARTESIAN_POINT('Ctrl Pts',(-19.1887826979866,23.8523255612065,-40.0703844562306));
#72465=CARTESIAN_POINT('Ctrl Pts',(-21.4468322987298,27.3829135588469,-39.8714975448559));
#72466=CARTESIAN_POINT('Ctrl Pts',(-25.6377467529413,27.3916110286012,-39.6726106334809));
#72467=CARTESIAN_POINT('Ctrl Pts',(-27.9104310081496,23.8704257331889,-39.4737237221061));
#72468=CARTESIAN_POINT('Ctrl Pts',(-26.1764809256665,20.0550284118138,-39.2748368107311));
#72469=CARTESIAN_POINT('Ctrl Pts',(-22.0292496165711,19.4514457104732,-39.0759498993563));
#72470=CARTESIAN_POINT('Ctrl Pts',(-19.2796910266931,22.6143189563253,-38.8770629879813));
#72471=CARTESIAN_POINT('Ctrl Pts',(-20.4544163760059,26.6372358038602,-38.6781760766065));
#72472=CARTESIAN_POINT('Ctrl Pts',(-24.4739526687759,27.8234767572942,-38.4792891652316));
#72473=CARTESIAN_POINT('Ctrl Pts',(-27.6446868524243,25.0829869570684,-38.2804022538567));
#72474=CARTESIAN_POINT('Ctrl Pts',(-27.0529830461042,20.9340441743723,-38.0815153424818));
#72475=CARTESIAN_POINT('Ctrl Pts',(-23.2425668796141,19.189175054166,-37.8826284311069));
#72476=CARTESIAN_POINT('Ctrl Pts',(-19.7148877399443,21.451766377414,-37.683741519732));
#72477=CARTESIAN_POINT('Ctrl Pts',(-19.711583658584,25.6426885541605,-37.4848546083571));
#72478=CARTESIAN_POINT('Ctrl Pts',(-23.2356908061633,27.9108394355789,-37.2859676969822));
#72479=CARTESIAN_POINT('Ctrl Pts',(-27.0488535090693,26.1719806691275,-37.0870807856073));
#72480=CARTESIAN_POINT('Ctrl Pts',(-27.6470985462135,22.0239760302641,-36.8881938742324));
#72481=CARTESIAN_POINT('Ctrl Pts',(-24.4806894512747,19.278490089308,-36.6893069628576));
#72482=CARTESIAN_POINT('Ctrl Pts',(-20.459287715283,20.4583916471769,-36.4904200514827));
#72483=CARTESIAN_POINT('Ctrl Pts',(-19.2782205749742,24.4794512113442,-36.2915331401078));
#72484=CARTESIAN_POINT('Ctrl Pts',(-22.0227885943122,27.6466559719694,-36.0926462287329));
#72485=CARTESIAN_POINT('Ctrl Pts',(-26.1709664645193,27.0496132887177,-35.893759317358));
#72486=CARTESIAN_POINT('Ctrl Pts',(-27.9109304303589,23.2369547666261,-35.6948724059831));
#72487=CARTESIAN_POINT('Ctrl Pts',(-25.6438011318411,19.712190327362,-35.4959854946082));
#72488=CARTESIAN_POINT('Ctrl Pts',(-21.4528781734377,19.7142796398676,-35.2970985832333));
#72489=CARTESIAN_POINT('Ctrl Pts',(-19.1892644222517,23.2413028030948,-35.0982116718584));
#72490=CARTESIAN_POINT('Ctrl Pts',(-20.9330289928265,27.0522245722874,-34.8993247604835));
#72491=CARTESIAN_POINT('Ctrl Pts',(-25.0818000916583,27.6451309544398,-34.7004378491086));
#72492=CARTESIAN_POINT('Ctrl Pts',(-27.8232088367022,24.4751912545249,-34.5015509377338));
#72493=CARTESIAN_POINT('Ctrl Pts',(-26.6381330243943,20.4553112902,-34.3026640263588));
#72494=CARTESIAN_POINT('Ctrl Pts',(-22.6155568483864,19.2794199190639,-34.103777114984));
#72495=CARTESIAN_POINT('Ctrl Pts',(-19.4518867562131,22.028061612044,-33.9048902036091));
#72496=CARTESIAN_POINT('Ctrl Pts',(-20.0542673275921,26.1754676996755,-33.7060032922341));
#72497=CARTESIAN_POINT('Ctrl Pts',(-23.869161890876,27.9105236294732,-33.5071163808593));
#72498=CARTESIAN_POINT('Ctrl Pts',(-27.3910057921265,25.6388601104361,-33.3082294694844));
#72499=CARTESIAN_POINT('Ctrl Pts',(-27.3835230892152,21.4479433112553,-33.1093425581096));
#72500=CARTESIAN_POINT('Ctrl Pts',(-23.853589751689,19.1888704392302,-32.9104556467346));
#72501=CARTESIAN_POINT('Ctrl Pts',(-20.0449152277426,20.9375379259584,-32.7115687353598));
#72502=CARTESIAN_POINT('Ctrl Pts',(-19.4573484825355,25.0870686136899,-32.5126818239848));
#72503=CARTESIAN_POINT('Ctrl Pts',(-22.6308135374686,27.8243956225835,-32.31379491261));
#72504=CARTESIAN_POINT('Ctrl Pts',(-26.6491650725236,26.6341475185233,-32.1149080012351));
#72505=CARTESIAN_POINT('Ctrl Pts',(-27.8198787270113,22.6100613927433,-31.9160210898602));
#72506=CARTESIAN_POINT('Ctrl Pts',(-25.0671679126064,19.4499312085962,-31.7171341784853));
#72507=CARTESIAN_POINT('Ctrl Pts',(-20.9205404763582,20.0576486704582,-31.5182472671104));
#72508=CARTESIAN_POINT('Ctrl Pts',(-19.1903954561497,23.8747729568218,-31.3193603557355));
#72509=CARTESIAN_POINT('Ctrl Pts',(-21.4665894334457,27.3936904872877,-31.1204734443606));
#72510=CARTESIAN_POINT('Ctrl Pts',(-25.6574931325347,27.3808144063633,-30.9215865329857));
#72511=CARTESIAN_POINT('Ctrl Pts',(-27.9120213839913,23.8479767407064,-30.7226996216109));
#72512=CARTESIAN_POINT('Ctrl Pts',(-26.1584538771994,20.0415557698175,-30.5238127102359));
#72513=CARTESIAN_POINT('Ctrl Pts',(-22.008170472895,19.4593296346659,-30.3249257988611));
#72514=CARTESIAN_POINT('Ctrl Pts',(-19.2749297336295,22.6363147888206,-30.1260388874862));
#72515=CARTESIAN_POINT('Ctrl Pts',(-20.4703481581894,26.653131239534,-29.9271519761113));
#72516=CARTESIAN_POINT('Ctrl Pts',(-24.4959375691721,27.8186652384729,-29.7282650647364));
#72517=CARTESIAN_POINT('Ctrl Pts',(-27.6525226115814,25.0618898615992,-29.5293781533615));
#72518=CARTESIAN_POINT('Ctrl Pts',(-27.0394692657196,20.9160479442529,-29.3304912419866));
#72519=CARTESIAN_POINT('Ctrl Pts',(-23.2201215780816,19.1908166990471,-29.1316043306117));
#72520=CARTESIAN_POINT('Ctrl Pts',(-19.7041362463246,21.4715373648386,-28.9327174192368));
#72521=CARTESIAN_POINT('Ctrl Pts',(-19.7224056839372,25.6624210229886,-28.7338305078619));
#72522=CARTESIAN_POINT('Ctrl Pts',(-23.2581418267462,27.9124009199948,-28.5349435964871));
#72523=CARTESIAN_POINT('Ctrl Pts',(-27.0623029404989,26.1539362973452,-28.3360566851121));
#72524=CARTESIAN_POINT('Ctrl Pts',(-27.6391875013296,22.0029070500411,-28.1371697737373));
#72525=CARTESIAN_POINT('Ctrl Pts',(-24.4586875095798,19.2737571071142,-27.9382828623624));
#72526=CARTESIAN_POINT('Ctrl Pts',(-20.4434127957375,20.4743438723577,-27.7393959509875));
#72527=CARTESIAN_POINT('Ctrl Pts',(-19.2830603826693,24.5014299014843,-27.5405090396126));
#72528=CARTESIAN_POINT('Ctrl Pts',(-22.0438957563241,27.6544645743154,-27.3416221282377));
#72529=CARTESIAN_POINT('Ctrl Pts',(-26.1889452885512,27.0360763597742,-27.1427352168628));
#72530=CARTESIAN_POINT('Ctrl Pts',(-27.9092599014785,23.2145115963496,-26.9438483054879));
#72531=CARTESIAN_POINT('Ctrl Pts',(-25.6240163244518,19.7014642863698,-26.744961394113));
#72532=CARTESIAN_POINT('Ctrl Pts',(-21.4331596480554,19.7251270504131,-26.5460744827382));
#72533=CARTESIAN_POINT('Ctrl Pts',(-19.1877318318474,23.2637558145954,-26.3471875713632));
#72534=CARTESIAN_POINT('Ctrl Pts',(-20.9510906580395,27.0656507708756,-26.1483006599883));
#72535=CARTESIAN_POINT('Ctrl Pts',(-25.1028588735346,27.6371928019669,-25.9494137486134));
#72536=CARTESIAN_POINT('Ctrl Pts',(-27.8279135001877,24.4531832400693,-25.7505268372386));
#72537=CARTESIAN_POINT('Ctrl Pts',(-26.6221603826357,20.4394569130743,-25.5516399258637));
#72538=CARTESIAN_POINT('Ctrl Pts',(-22.593584404903,19.2842880076173,-25.3527530144888));
#72539=CARTESIAN_POINT('Ctrl Pts',(-19.4441053236104,22.0491788056415,-25.1538661031139));
#72540=CARTESIAN_POINT('Ctrl Pts',(-20.0678273826751,26.193429087844,-24.954979191739));
#72541=CARTESIAN_POINT('Ctrl Pts',(-23.8916028927267,27.9088242193601,-24.7560922803641));
#72542=CARTESIAN_POINT('Ctrl Pts',(-27.4017063627272,25.6190615158492,-24.5572053689893));
#72543=CARTESIAN_POINT('Ctrl Pts',(-27.3726503114427,21.428238761976,-24.3583184576143));
#72544=CARTESIAN_POINT('Ctrl Pts',(-23.8311347864567,19.1873667453757,-24.1594315462395));
#72545=CARTESIAN_POINT('Ctrl Pts',(-20.0315122842318,20.9556168546889,-23.9605446348646));
#72546=CARTESIAN_POINT('Ctrl Pts',(-19.4653137294506,25.1081171623423,-23.7616577234897));
#72547=CARTESIAN_POINT('Ctrl Pts',(-22.6528275882359,27.8290719595691,-23.5627708121148));
#72548=CARTESIAN_POINT('Ctrl Pts',(-26.6649988809719,26.6181544866401,-23.3638839007399));
#72549=CARTESIAN_POINT('Ctrl Pts',(-27.814982365662,22.5880952323066,-23.164996989365));
#72550=CARTESIAN_POINT('Ctrl Pts',(-25.0460407223967,19.4421769586241,-22.9661100779901));
#72551=CARTESIAN_POINT('Ctrl Pts',(-20.9025965538004,20.0712318292229,-22.7672231666153));
#72552=CARTESIAN_POINT('Ctrl Pts',(-19.1921237446807,23.8972117530806,-22.5683362552403));
#72553=CARTESIAN_POINT('Ctrl Pts',(-21.4864017824403,27.4043655697748,-22.3694493438655));
#72554=CARTESIAN_POINT('Ctrl Pts',(-25.6771836730771,27.369916279371,-22.1705624324905));
#72555=CARTESIAN_POINT('Ctrl Pts',(-27.9134961788053,23.8255198589316,-21.9716755211157));
#72556=CARTESIAN_POINT('Ctrl Pts',(-26.1403577148932,20.0281761035817,-21.7727886097408));
#72557=CARTESIAN_POINT('Ctrl Pts',(-21.9871321923262,19.4673219628314,-21.5739016983659));
#72558=CARTESIAN_POINT('Ctrl Pts',(-19.2702817308889,22.6583348394408,-21.375014786991));
#72559=CARTESIAN_POINT('Ctrl Pts',(-20.4863615537098,26.6689444530814,-21.1761278756161));
#72560=CARTESIAN_POINT('Ctrl Pts',(-24.5178974101823,27.8137406124369,-20.9772409642412));
#72561=CARTESIAN_POINT('Ctrl Pts',(-27.6602496660805,25.0407527097676,-20.7783540528663));
#72562=CARTESIAN_POINT('Ctrl Pts',(-27.025863025769,20.8981215170238,-20.5794671414914));
#72563=CARTESIAN_POINT('Ctrl Pts',(-23.1976850245772,19.1925738631339,-20.3805802301165));
#72564=CARTESIAN_POINT('Ctrl Pts',(-19.6934866696307,21.4913634354284,-20.1816933187417));
#72565=CARTESIAN_POINT('Ctrl Pts',(-19.7333291421004,25.682097522183,-19.9828064073668));
#72566=CARTESIAN_POINT('Ctrl Pts',(-23.2806005878712,27.9138468133262,-19.7839194959919));
#72567=CARTESIAN_POINT('Ctrl Pts',(-27.0756593073007,26.1358229314335,-19.585032584617));
#72568=CARTESIAN_POINT('Ctrl Pts',(-27.6311681051505,21.981879072399,-19.3861456732421));
#72569=CARTESIAN_POINT('Ctrl Pts',(-24.4366614955757,19.2691374463162,-19.1872587618672));
#72570=CARTESIAN_POINT('Ctrl Pts',(-20.4276202032802,20.4903776049946,-18.9883718504923));
#72571=CARTESIAN_POINT('Ctrl Pts',(-19.288013265236,24.523383386699,-18.7894849391174));
#72572=CARTESIAN_POINT('Ctrl Pts',(-22.0650428347712,27.6621644205442,-18.5905980277425));
#72573=CARTESIAN_POINT('Ctrl Pts',(-26.2068541907623,27.0224470611721,-18.3917111163676));
#72574=CARTESIAN_POINT('Ctrl Pts',(-27.9074738647463,23.1920773227581,-18.1928242049927));
#72575=CARTESIAN_POINT('Ctrl Pts',(-25.6041765651021,19.6908402331065,-17.9939372936179));
#72576=CARTESIAN_POINT('Ctrl Pts',(-21.4134972227966,19.7360758216561,-17.795050382243));
#72577=CARTESIAN_POINT('Ctrl Pts',(-19.1863148423934,23.2862164178749,-17.5961634708681));
#72578=CARTESIAN_POINT('Ctrl Pts',(-20.9692211975579,27.078983816123,-17.3972765594932));
#72579=CARTESIAN_POINT('Ctrl Pts',(-25.123876513424,27.6291463510555,-17.1983896481183));
#72580=CARTESIAN_POINT('Ctrl Pts',(-27.832504811392,24.4311512991602,-16.9995027367434));
#72581=CARTESIAN_POINT('Ctrl Pts',(-26.6061063394368,20.4236849678625,-16.8006158253685));
#72582=CARTESIAN_POINT('Ctrl Pts',(-22.5716373118425,19.2892691385119,-16.6017289139936));
#72583=CARTESIAN_POINT('Ctrl Pts',(-19.4364326984041,22.0703357756807,-16.4028420026187));
#72584=CARTESIAN_POINT('Ctrl Pts',(-20.0814797173563,26.211320435377,-16.2039550912438));
#72585=CARTESIAN_POINT('Ctrl Pts',(-23.9140348492504,27.9070093129403,-16.005068179869));
#72586=CARTESIAN_POINT('Ctrl Pts',(-27.4123048749644,25.5992081005977,-15.8061812684941));
#72587=CARTESIAN_POINT('Ctrl Pts',(-27.3616762452531,21.4085904432168,-15.6072943571192));
#72588=CARTESIAN_POINT('Ctrl Pts',(-23.808672378221,19.185978662146,-15.4084074457443));
#72589=CARTESIAN_POINT('Ctrl Pts',(-20.0182025826206,20.9737645377867,-15.2095205343694));
#72590=CARTESIAN_POINT('Ctrl Pts',(-19.4733872217679,25.1291244296706,-15.0106336229945));
#72591=CARTESIAN_POINT('Ctrl Pts',(-22.6748654195614,27.8336349135756,-14.8117467116196));
#72592=CARTESIAN_POINT('Ctrl Pts',(-26.6807501528174,26.6020801594677,-14.6128598002447));
#72593=CARTESIAN_POINT('Ctrl Pts',(-27.8099729946892,22.5661545677486,-14.4139728888698));
#72594=CARTESIAN_POINT('Ctrl Pts',(-25.0248738958048,19.4345315671475,-14.2150859774949));
#72595=CARTESIAN_POINT('Ctrl Pts',(-20.8847227905765,20.0849071773727,-14.01619906612));
#72596=CARTESIAN_POINT('Ctrl Pts',(-19.1939675177824,23.9196413553853,-13.8173121547452));
#72597=CARTESIAN_POINT('Ctrl Pts',(-21.5062688207131,27.4149385234332,-13.6184252433703));
#72598=CARTESIAN_POINT('Ctrl Pts',(-25.6968178527955,27.3589169364095,-13.4195383319954));
#72599=CARTESIAN_POINT('Ctrl Pts',(-27.9148553535118,23.8030556829416,-13.2206514206205));
#72600=CARTESIAN_POINT('Ctrl Pts',(-26.1221929182718,20.0148897676498,-13.0217645092456));
#72601=CARTESIAN_POINT('Ctrl Pts',(-21.9661353323509,19.4754224831835,-12.8228775978707));
#72602=CARTESIAN_POINT('Ctrl Pts',(-19.2657471416371,22.6803785246842,-12.6239906864958));
#72603=CARTESIAN_POINT('Ctrl Pts',(-20.5024561382339,26.6846750254737,-12.4251037751209));
#72604=CARTESIAN_POINT('Ctrl Pts',(-24.5398316099007,27.8087030096821,-12.226216863746));
#72605=CARTESIAN_POINT('Ctrl Pts',(-27.6678678111651,25.019576061679,-12.0273299523711));
#72606=CARTESIAN_POINT('Ctrl Pts',(-27.0121646867995,20.8802653677112,-11.8284430409963));
#72607=CARTESIAN_POINT('Ctrl Pts',(-23.1752578136387,19.1944464998637,-11.6295561296213));
#72608=CARTESIAN_POINT('Ctrl Pts',(-19.682939292062,21.5112440638194,-11.4306692182465));
#72609=CARTESIAN_POINT('Ctrl Pts',(-19.7443537436168,25.701717530343,-11.2317823068716));
#72610=CARTESIAN_POINT('Ctrl Pts',(-23.3030664944112,27.9151770772588,-11.0328953954967));
#72611=CARTESIAN_POINT('Ctrl Pts',(-27.0889222555488,26.1176410513722,-10.8340084841218));
#72612=CARTESIAN_POINT('Ctrl Pts',(-27.6230405701793,21.9608926545511,-10.6351215727469));
#72613=CARTESIAN_POINT('Ctrl Pts',(-24.4146119929223,19.264631229329,-10.436234661372));
#72614=CARTESIAN_POINT('Ctrl Pts',(-20.4119103563936,20.5064924202153,-10.2373477499971));
#72615=CARTESIAN_POINT('Ctrl Pts',(-19.2930790914296,24.5453110852506,-10.0384608386222));
#72616=CARTESIAN_POINT('Ctrl Pts',(-22.0862292692843,27.6697553066202,-9.83957392724733));
#72617=CARTESIAN_POINT('Ctrl Pts',(-26.2246926965909,27.0087257540695,-9.64068701587243));
#72618=CARTESIAN_POINT('Ctrl Pts',(-27.9055723674896,23.1696525403292,-9.44180010449755));
#72619=CARTESIAN_POINT('Ctrl Pts',(-25.5842823795188,19.6803184490956,-9.24291319312266));
#72620=CARTESIAN_POINT('Ctrl Pts',(-21.3938914186887,19.7471256634687,-9.04402628174778));
#72621=CARTESIAN_POINT('Ctrl Pts',(-19.1850134914383,23.3086840177575,-8.84513937037286));
#72622=CARTESIAN_POINT('Ctrl Pts',(-20.9874201309466,27.0922233547217,-8.64625245899801));
#72623=CARTESIAN_POINT('Ctrl Pts',(-25.1448524543876,27.6209918149259,-8.44736554762308));
#72624=CARTESIAN_POINT('Ctrl Pts',(-27.8369826486513,24.4090960156147,-8.24847863624822));
#72625=CARTESIAN_POINT('Ctrl Pts',(-26.5899713202086,20.4079958724997,-8.0495917248733));
#72626=CARTESIAN_POINT('Ctrl Pts',(-22.5497161507734,19.2943631797545,-7.85070481349842));
#72627=CARTESIAN_POINT('Ctrl Pts',(-19.4288690839087,22.0915319615302,-7.65181790212353));
#72628=CARTESIAN_POINT('Ctrl Pts',(-20.0952239698672,26.2291412681779,-7.45293099074865));
#72629=CARTESIAN_POINT('Ctrl Pts',(-23.9364571660305,27.905078958306,-7.25404407937375));
#72630=CARTESIAN_POINT('Ctrl Pts',(-27.4228010479919,25.5793003907701,-7.05515716799886));
#72631=CARTESIAN_POINT('Ctrl Pts',(-27.3506011814443,21.388998875632,-6.85627025662397));
#72632=CARTESIAN_POINT('Ctrl Pts',(-23.7862031222059,19.1847062263234,-6.65738334524908));
#72633=CARTESIAN_POINT('Ctrl Pts',(-20.0049864755982,20.9919804943623,-6.45849643387418));
#72634=CARTESIAN_POINT('Ctrl Pts',(-19.4815687455506,25.1500898590101,-6.25960952249932));
#72635=CARTESIAN_POINT('Ctrl Pts',(-22.6969264474718,27.838084363691,-6.0607226111244));
#72636=CARTESIAN_POINT('Ctrl Pts',(-26.6964184706725,26.5859249629543,-5.86183569974952));
#72637=CARTESIAN_POINT('Ctrl Pts',(-27.8048507468344,22.5442399804672,-5.66294878837463));
#72638=CARTESIAN_POINT('Ctrl Pts',(-25.0036679937236,19.4269952367594,-5.46406187699974));
#72639=CARTESIAN_POINT('Ctrl Pts',(-20.8669196603177,20.0986743525289,-5.26517496562485));
#72640=CARTESIAN_POINT('Ctrl Pts',(-19.1959267265971,23.9420611693814,-5.06628805424996));
#72641=CARTESIAN_POINT('Ctrl Pts',(-21.5261900218144,27.4254090680936,-4.86740114287507));
#72642=CARTESIAN_POINT('Ctrl Pts',(-25.7163951514103,27.347816668947,-4.66851423150017));
#72643=CARTESIAN_POINT('Ctrl Pts',(-27.9160988720948,23.7805848080068,-4.46962732012529));
#72644=CARTESIAN_POINT('Ctrl Pts',(-26.1039599686777,20.0016971140919,-4.27074040875039));
#72645=CARTESIAN_POINT('Ctrl Pts',(-21.9451804493579,19.4836309810696,-4.07185349737551));
#72646=CARTESIAN_POINT('Ctrl Pts',(-19.2613260860344,22.7024452604228,-3.87296658600062));
#72647=CARTESIAN_POINT('Ctrl Pts',(-20.518631485277,26.7003225398718,-3.67407967462572));
#72648=CARTESIAN_POINT('Ctrl Pts',(-24.5617395870999,27.8035525636983,-3.47519276325084));
#72649=CARTESIAN_POINT('Ctrl Pts',(-27.6753768449648,24.9983604784866,-3.27630585187594));
#72650=CARTESIAN_POINT('Ctrl Pts',(-26.9983746117987,20.8624799694792,-3.07741894050105));
#72651=CARTESIAN_POINT('Ctrl Pts',(-23.1528405395576,19.1964345596142,-2.87853202912616));
#72652=CARTESIAN_POINT('Ctrl Pts',(-19.6724943931097,21.5311787232013,-2.67964511775127));
#72653=CARTESIAN_POINT('Ctrl Pts',(-19.755479196349,25.7212805275649,-2.48075820637638));
#72654=CARTESIAN_POINT('Ctrl Pts',(-23.3255389510499,27.9163916765421,-2.28187129500149));
#72655=CARTESIAN_POINT('Ctrl Pts',(-27.102091433793,26.0993911389568,-2.0829843836266));
#72656=CARTESIAN_POINT('Ctrl Pts',(-27.6148051117849,21.9399483526093,-1.88409747225172));
#72657=CARTESIAN_POINT('Ctrl Pts',(-24.3925395859019,19.2602385755614,-1.68521056087682));
#72658=CARTESIAN_POINT('Ctrl Pts',(-20.3962836713676,20.5226878909986,-1.48632364950193));
#72659=CARTESIAN_POINT('Ctrl Pts',(-19.2982577270124,24.5672124160846,-1.28743673812705));
#72660=CARTESIAN_POINT('Ctrl Pts',(-22.1074544984513,27.677237031395,-1.08854982675215));
#72661=CARTESIAN_POINT('Ctrl Pts',(-26.2424603333401,26.9949128020628,-0.88966291537726));
#72662=CARTESIAN_POINT('Ctrl Pts',(-27.9035554600959,23.14723784329,-0.690776004002363));
#72663=CARTESIAN_POINT('Ctrl Pts',(-25.5643342948712,19.6698992131499,-0.491889092627479));
#72664=CARTESIAN_POINT('Ctrl Pts',(-21.3743427552598,19.7582762830453,-0.293002181252585));
#72665=CARTESIAN_POINT('Ctrl Pts',(-19.1838278134659,23.331158018882,-0.0941152698776977));
#72666=CARTESIAN_POINT('Ctrl Pts',(-21.0056869759584,27.1053690358419,0.104771641497192));
#72667=CARTESIAN_POINT('Ctrl Pts',(-25.1657861405909,27.6127294096622,0.303658552872082));
#72668=CARTESIAN_POINT('Ctrl Pts',(-27.8413468933091,24.3870179738681,0.502545464246976));
#72669=CARTESIAN_POINT('Ctrl Pts',(-26.5737557525075,20.392390042726,0.701432375621864));
#72670=CARTESIAN_POINT('Ctrl Pts',(-22.5278215025772,19.2995699963595,0.900319286996756));
#72671=CARTESIAN_POINT('Ctrl Pts',(-19.4214146805498,22.1127668015191,1.09920619837165));
#72672=CARTESIAN_POINT('Ctrl Pts',(-20.1090597760031,26.2468911140184,1.29809310974654));
#72673=CARTESIAN_POINT('Ctrl Pts',(-23.9588692489054,27.9030332066094,1.49698002112143));
#72674=CARTESIAN_POINT('Ctrl Pts',(-27.4331946036748,25.5593389138944,1.69586693249632));
#72675=CARTESIAN_POINT('Ctrl Pts',(-27.3394254134909,21.3694645783718,1.89475384387121));
#72676=CARTESIAN_POINT('Ctrl Pts',(-23.7637276138164,19.1835494716255,2.0936407552461));
#72677=CARTESIAN_POINT('Ctrl Pts',(-19.9918643133737,21.0102642417176,2.292527666621));
#72678=CARTESIAN_POINT('Ctrl Pts',(-19.4898580839996,25.1710128948049,2.49141457799587));
#72679=CARTESIAN_POINT('Ctrl Pts',(-22.7190100873796,27.8424201920111,2.69030148937078));
#72680=CARTESIAN_POINT('Ctrl Pts',(-26.7120034193478,26.5696893251909,2.88918840074566));
#72681=CARTESIAN_POINT('Ctrl Pts',(-27.7996157578303,22.5223520511699,3.08807531212054));
#72682=CARTESIAN_POINT('Ctrl Pts',(-24.9824235780812,19.4195681671619,3.28696222349545));
#72683=CARTESIAN_POINT('Ctrl Pts',(-20.8491876347826,20.1125329898798,3.48584913487033));
#72684=CARTESIAN_POINT('Ctrl Pts',(-19.1980013192086,23.9644706009737,3.68473604624521));
#72685=CARTESIAN_POINT('Ctrl Pts',(-21.5461648578586,27.4357769263005,3.88362295762013));
#72686=CARTESIAN_POINT('Ctrl Pts',(-25.7359150501498,27.3366157711258,4.082509868995));
#72687=CARTESIAN_POINT('Ctrl Pts',(-27.9172267016021,23.7581078295755,4.2813967803699));
#72688=CARTESIAN_POINT('Ctrl Pts',(-26.0856593492601,19.9885984924956,4.48028369174478));
#72689=CARTESIAN_POINT('Ctrl Pts',(-21.9242680986235,19.4919472389751,4.67917060311969));
#72690=CARTESIAN_POINT('Ctrl Pts',(-19.2570186812331,22.7245344619175,4.87805751449454));
#72691=CARTESIAN_POINT('Ctrl Pts',(-20.5348871662136,26.7158865816374,5.07694442586947));
#72692=CARTESIAN_POINT('Ctrl Pts',(-24.5836207612481,27.7982894109654,5.27583133724435));
#72693=CARTESIAN_POINT('Ctrl Pts',(-27.6827765685001,24.9771065223749,5.47471824861922));
#72694=CARTESIAN_POINT('Ctrl Pts',(-26.9844931661851,20.8447657936171,5.67360515999414));
#72695=CARTESIAN_POINT('Ctrl Pts',(-23.1304337963616,19.1985379897045,5.87249207136902));
#72696=CARTESIAN_POINT('Ctrl Pts',(-19.6621522495498,21.5511668853325,6.0713789827439));
#72697=CARTESIAN_POINT('Ctrl Pts',(-19.7667052054878,25.7407859954551,6.2702658941188));
#72698=CARTESIAN_POINT('Ctrl Pts',(-23.3480173622973,27.9174905789912,6.46915280549369));
#72699=CARTESIAN_POINT('Ctrl Pts',(-27.1151664930678,26.0810736777856,6.66803971686857));
#72700=CARTESIAN_POINT('Ctrl Pts',(-27.6064619481956,21.9190467215694,6.86692662824348));
#72701=CARTESIAN_POINT('Ctrl Pts',(-24.3704448594037,19.2559596014127,7.06581353961836));
#72702=CARTESIAN_POINT('Ctrl Pts',(-20.3807405622883,20.5389635881862,7.26470045099325));
#72703=CARTESIAN_POINT('Ctrl Pts',(-19.3035490347575,24.5890867988448,7.46358736236814));
#72704=CARTESIAN_POINT('Ctrl Pts',(-22.128717959832,27.6846093966129,7.66247427374303));
#72705=CARTESIAN_POINT('Ctrl Pts',(-26.2601566301919,26.9810085711767,7.86136118511791));
#72706=CARTESIAN_POINT('Ctrl Pts',(-27.9014231960102,23.1248338255997,8.06024809649283));
#72707=CARTESIAN_POINT('Ctrl Pts',(-25.544332839757,19.6595828013654,8.2591350078677));
#72708=CARTESIAN_POINT('Ctrl Pts',(-21.3548517505231,19.769527384909,8.45802191924259));
#72709=CARTESIAN_POINT('Ctrl Pts',(-19.182757839895,23.3536378257174,8.65690883061749));
#72710=CARTESIAN_POINT('Ctrl Pts',(-21.0240212485464,27.1184205111404,8.85579574199238));
#72711=CARTESIAN_POINT('Ctrl Pts',(-25.1866770173191,27.6043593542072,9.05468265336725));
#72712=CARTESIAN_POINT('Ctrl Pts',(-27.8455974297187,24.3649177589591,9.25356956474216));
#72713=CARTESIAN_POINT('Ctrl Pts',(-26.557460066024,20.3768678920752,9.45245647611703));
#72714=CARTESIAN_POINT('Ctrl Pts',(-22.5059539474326,19.3048894503536,9.65134338749194));
#72715=CARTESIAN_POINT('Ctrl Pts',(-19.4140696858589,22.1340397329529,9.85023029886681));
#72716=CARTESIAN_POINT('Ctrl Pts',(-20.1229867691341,26.2645695025515,10.0491172102417));
#72717=CARTESIAN_POINT('Ctrl Pts',(-23.9812705039851,27.9008721120599,10.2480041216166));
#72718=CARTESIAN_POINT('Ctrl Pts',(-27.4434852665982,25.5393241989229,10.4468910329915));
#72719=CARTESIAN_POINT('Ctrl Pts',(-27.3281492375358,21.3499880690689,10.6457779443664));
#72720=CARTESIAN_POINT('Ctrl Pts',(-23.7412464486233,19.1825084287052,10.8446648557413));
#72721=CARTESIAN_POINT('Ctrl Pts',(-19.9788364436668,21.0286152953575,11.0435517671161));
#72722=CARTESIAN_POINT('Ctrl Pts',(-19.4982550174582,25.191892982623,11.242438678491));
#72723=CARTESIAN_POINT('Ctrl Pts',(-22.7411157540979,27.8466422836418,11.4413255898659));
#72724=CARTESIAN_POINT('Ctrl Pts',(-26.727504585863,26.5533736764001,11.6402125012408));
#72725=CARTESIAN_POINT('Ctrl Pts',(-27.7942681663972,22.5004913598574,11.8390994126157));
#72726=CARTESIAN_POINT('Ctrl Pts',(-24.9611412118258,19.4122505551629,12.0379863239906));
#72727=CARTESIAN_POINT('Ctrl Pts',(-20.8315271838466,20.1264827221902,12.2368732353655));
#72728=CARTESIAN_POINT('Ctrl Pts',(-19.2001912406427,23.9868690563425,12.4357601467404));
#72729=CARTESIAN_POINT('Ctrl Pts',(-21.5661927995398,27.4460418233196,12.6346470581153));
#72730=CARTESIAN_POINT('Ctrl Pts',(-25.7553770317623,27.3253145397543,12.8335339694901));
#72731=CARTESIAN_POINT('Ctrl Pts',(-27.918238812148,23.7356253432576,13.0324208808651));
#72732=CARTESIAN_POINT('Ctrl Pts',(-26.0672915449605,19.9755942499566,13.2313077922399));
#72733=CARTESIAN_POINT('Ctrl Pts',(-21.9033988342966,19.5003710365307,13.4301947036148));
#72734=CARTESIAN_POINT('Ctrl Pts',(-19.2528250413737,22.7466455438341,13.6290816149897));
#72735=CARTESIAN_POINT('Ctrl Pts',(-20.5512227502902,26.7313667383445,13.8279685263646));
#72736=CARTESIAN_POINT('Ctrl Pts',(-24.6054745525237,27.7929136909498,14.0268554377395));
#72737=CARTESIAN_POINT('Ctrl Pts',(-27.6900667856881,24.9558147565452,14.2257423491144));
#72738=CARTESIAN_POINT('Ctrl Pts',(-26.9705207177986,20.8271233095267,14.4246292604893));
#72739=CARTESIAN_POINT('Ctrl Pts',(-23.1080381777993,19.2007567343966,14.6235161718642));
#72740=CARTESIAN_POINT('Ctrl Pts',(-19.6519131354353,21.5712080205535,14.8224030832391));
#72741=CARTESIAN_POINT('Ctrl Pts',(-19.7780314735584,25.760233417145,15.0212899946139));
#72742=CARTESIAN_POINT('Ctrl Pts',(-23.3705011325054,27.9184737554865,15.2201769059889));
#72743=CARTESIAN_POINT('Ctrl Pts',(-27.1281470869014,26.0626891532467,15.4190638173638));
#72744=CARTESIAN_POINT('Ctrl Pts',(-27.5980113004945,21.898188315297,15.6179507287386));
#72745=CARTESIAN_POINT('Ctrl Pts',(-24.3483283989083,19.2517944202697,15.8168376401135));
#72746=CARTESIAN_POINT('Ctrl Pts',(-20.3652814410273,20.5553190804943,16.0157245514884));
#72747=CARTESIAN_POINT('Ctrl Pts',(-19.3089528744526,24.6109336538896,16.2146114628633));
#72748=CARTESIAN_POINT('Ctrl Pts',(-22.1500190899732,27.6918722069163,16.4134983742382));
#72749=CARTESIAN_POINT('Ctrl Pts',(-26.2777811182176,26.9670134298545,16.6123852856131));
#72750=CARTESIAN_POINT('Ctrl Pts',(-27.899175631735,23.1024410809349,16.811272196988));
#72751=CARTESIAN_POINT('Ctrl Pts',(-25.5242785441877,19.6493694871132,17.0101591083628));
#72752=CARTESIAN_POINT('Ctrl Pts',(-21.335418920964,19.7808786709211,17.2090460197378));
#72753=CARTESIAN_POINT('Ctrl Pts',(-19.1818035990787,23.3761228425789,17.4079329311126));
#72754=CARTESIAN_POINT('Ctrl Pts',(-21.0424224628768,27.1313774347708,17.6068198424875));
#72755=CARTESIAN_POINT('Ctrl Pts',(-25.2075245309924,27.5958818703561,17.8057067538624));
#72756=CARTESIAN_POINT('Ctrl Pts',(-27.8497341452466,24.3427959565135,18.0045936652373));
#72757=CARTESIAN_POINT('Ctrl Pts',(-26.5410846925722,20.3614298318631,18.2034805766122));
#72758=CARTESIAN_POINT('Ctrl Pts',(-22.4841140648005,19.3103214007783,18.4023674879871));
#72759=CARTESIAN_POINT('Ctrl Pts',(-19.4068342944688,22.1553501921275,18.601254399362));
#72760=CARTESIAN_POINT('Ctrl Pts',(-20.1370045802135,26.2821759653235,18.8001413107369));
#72761=CARTESIAN_POINT('Ctrl Pts',(-24.0036603376662,27.8985957319239,18.9990282221118));
#72762=CARTESIAN_POINT('Ctrl Pts',(-27.4536727640731,25.5192567762184,19.1979151334866));
#72763=CARTESIAN_POINT('Ctrl Pts',(-27.3167729523822,21.3305698638249,19.3968020448616));
#72764=CARTESIAN_POINT('Ctrl Pts',(-23.7187602223476,19.1815831251482,19.5956889562364));
#72765=CARTESIAN_POINT('Ctrl Pts',(-19.9659032116986,21.0470331690039,19.7945758676113));
#72766=CARTESIAN_POINT('Ctrl Pts',(-19.5067593234192,25.2127295691698,19.9934627789862));
#72767=CARTESIAN_POINT('Ctrl Pts',(-22.7632428618561,27.8507505267037,20.1923496903611));
#72768=CARTESIAN_POINT('Ctrl Pts',(-26.7429215594582,26.5369784489248,20.391236601736));
#72769=CARTESIAN_POINT('Ctrl Pts',(-27.7888081142389,22.4786584858086,20.5901235131109));
#72770=CARTESIAN_POINT('Ctrl Pts',(-24.9398214589118,19.4050425946691,20.7890104244858));
#72771=CARTESIAN_POINT('Ctrl Pts',(-20.8139387754876,20.1405231798108,20.9878973358607));
#72772=CARTESIAN_POINT('Ctrl Pts',(-19.2024964328697,24.0092559419588,21.1867842472355));
#72773=CARTESIAN_POINT('Ctrl Pts',(-21.586273316144,27.4562034871449,21.3856711586105));
#72774=CARTESIAN_POINT('Ctrl Pts',(-25.7747805805317,27.3139132743005,21.5845580699853));
#72775=CARTESIAN_POINT('Ctrl Pts',(-27.919135176913,23.7131379448084,21.7834449813602));
#72776=CARTESIAN_POINT('Ctrl Pts',(-26.0488570425013,19.9626847310703,21.9823318927351));
#72777=CARTESIAN_POINT('Ctrl Pts',(-21.8825732093851,19.5089021505166,22.18121880411));
#72778=CARTESIAN_POINT('Ctrl Pts',(-19.2487452775818,22.768777920259,22.3801057154849));
#72779=CARTESIAN_POINT('Ctrl Pts',(-20.5676378046356,26.746762599789,22.5789926268598));
#72780=CARTESIAN_POINT('Ctrl Pts',(-24.6273003818304,27.7874255461016,22.7778795382347));
#72781=CARTESIAN_POINT('Ctrl Pts',(-27.6972473033478,24.9344857451995,22.9767664496096));
#72782=CARTESIAN_POINT('Ctrl Pts',(-26.9564576368906,20.8095529847125,23.1756533609844));
#72783=CARTESIAN_POINT('Ctrl Pts',(-23.0856542773232,19.2030907348922,23.3745402723594));
#72784=CARTESIAN_POINT('Ctrl Pts',(-19.6417773220915,21.5913015978093,23.5734271837343));
#72785=CARTESIAN_POINT('Ctrl Pts',(-19.7894577004254,25.7796222772883,23.7723140951091));
#72786=CARTESIAN_POINT('Ctrl Pts',(-23.3929896658942,27.9193411800047,23.9712010064841));
#72787=CARTESIAN_POINT('Ctrl Pts',(-27.1410328713078,26.0442380524495,24.1700879178589));
#72788=CARTESIAN_POINT('Ctrl Pts',(-27.5894533926459,21.8773736866169,24.3689748292338));
#72789=CARTESIAN_POINT('Ctrl Pts',(-24.3261907904083,19.2477431423055,24.5678617406087));
#72790=CARTESIAN_POINT('Ctrl Pts',(-20.3499067173511,20.5717539348997,24.7667486519836));
#72791=CARTESIAN_POINT('Ctrl Pts',(-19.314469102675,24.6327524015971,24.9656355633585));
#72792=CARTESIAN_POINT('Ctrl Pts',(-22.1713573248539,27.6990252711903,25.1645224747334));
#72793=CARTESIAN_POINT('Ctrl Pts',(-26.2953333295803,26.9529277464185,25.3634093861082));
#72794=CARTESIAN_POINT('Ctrl Pts',(-27.8968128283606,23.080060207451,25.5622962974831));
#72795=CARTESIAN_POINT('Ctrl Pts',(-25.5041719366806,19.6392595320107,25.761183208858));
#72796=CARTESIAN_POINT('Ctrl Pts',(-21.316044786992,19.7923298573219,25.960070120233));
#72797=CARTESIAN_POINT('Ctrl Pts',(-19.1809651059832,23.398612441479,26.1589570316078));
#72798=CARTESIAN_POINT('Ctrl Pts',(-21.0608901508285,27.1442395241256,26.3578439429827));
#72799=CARTESIAN_POINT('Ctrl Pts',(-25.2283280923853,27.5872970680732,26.5567308543576));
#72800=CARTESIAN_POINT('Ctrl Pts',(-27.85375699975,24.320653369264,26.7556177657325));
#72801=CARTESIAN_POINT('Ctrl Pts',(-26.524629934895,20.3460758623164,26.9545046771074));
#72802=CARTESIAN_POINT('Ctrl Pts',(-22.4623026811071,19.3158664757075,27.1533915884823));
#72803=CARTESIAN_POINT('Ctrl Pts',(-19.399708230402,22.1766961566261,27.3522784998572));
#72804=CARTESIAN_POINT('Ctrl Pts',(-20.1511137209111,26.2997127882555,27.5511654112321));
#72805=CARTESIAN_POINT('Ctrl Pts',(-24.0260364891328,27.8961989293013,27.750052322607));
#72806=CARTESIAN_POINT('Ctrl Pts',(-27.4637599747539,25.4991469909509,27.9489392339819));
#72807=CARTESIAN_POINT('Ctrl Pts',(-27.3052909142717,21.3111919474789,28.1478261453567));
#72808=CARTESIAN_POINT('Ctrl Pts',(-23.6962807566228,19.1808085733704,28.3467130567316));
#72809=CARTESIAN_POINT('Ctrl Pts',(-19.9530437635938,21.0654513101587,28.5455999681065));
#72810=CARTESIAN_POINT('Ctrl Pts',(-19.5154108002811,25.2336468469387,28.7444868794814));
#72811=CARTESIAN_POINT('Ctrl Pts',(-22.7853152490305,27.854509256677,28.9433737908563));
#72812=CARTESIAN_POINT('Ctrl Pts',(-26.7583966519409,26.5209489557215,29.1422607022312));
#72813=CARTESIAN_POINT('Ctrl Pts',(-27.782966107073,22.456013156451,29.3411476136061));
#72814=CARTESIAN_POINT('Ctrl Pts',(-24.9189752763196,19.3995389604751,29.540034524981));
#72815=CARTESIAN_POINT('Ctrl Pts',(-20.7954488425069,20.151587834895,29.7389214363559));
#72816=CARTESIAN_POINT('Ctrl Pts',(-19.206841997626,24.0378700261007,29.9378083477307));
#72817=CARTESIAN_POINT('Ctrl Pts',(-20.8035465588388,26.3133894497781,30.0703996219807));
#72818=CARTESIAN_POINT('Ctrl Pts',(-21.9068279226878,26.8610413387076,30.1366952591057));
#72819=CARTESIAN_POINT('Ctrl Pts',(-21.5447307071333,20.7349338698167,-75.1351504332081));
#72820=CARTESIAN_POINT('Ctrl Pts',(-20.6058873997063,21.4036543954464,-75.0688106032636));
#72821=CARTESIAN_POINT('Ctrl Pts',(-19.4669883124013,23.7419128688188,-74.9361751361943));
#72822=CARTESIAN_POINT('Ctrl Pts',(-21.5093735067961,27.0961553314539,-74.7372440319998));
#72823=CARTESIAN_POINT('Ctrl Pts',(-25.4282714863658,27.1804579122132,-74.538357120625));
#72824=CARTESIAN_POINT('Ctrl Pts',(-27.6206045269464,23.9343746038397,-74.33947020925));
#72825=CARTESIAN_POINT('Ctrl Pts',(-26.0730651857951,20.332453394204,-74.1405832978753));
#72826=CARTESIAN_POINT('Ctrl Pts',(-22.2070441073339,19.6889287249836,-73.9416963865003));
#72827=CARTESIAN_POINT('Ctrl Pts',(-19.5754399103481,22.5928329886891,-73.7428094751254));
#72828=CARTESIAN_POINT('Ctrl Pts',(-20.5962867745515,26.3769483984124,-73.5439225637506));
#72829=CARTESIAN_POINT('Ctrl Pts',(-24.3316119952896,27.5633455521573,-73.3450356523755));
#72830=CARTESIAN_POINT('Ctrl Pts',(-27.3489159621601,25.0621693264582,-73.1461487410009));
#72831=CARTESIAN_POINT('Ctrl Pts',(-26.875579925032,21.1716068112945,-72.9472618296257));
#72832=CARTESIAN_POINT('Ctrl Pts',(-23.3465448625251,19.4668513729129,-72.7483749182512));
#72833=CARTESIAN_POINT('Ctrl Pts',(-20.0047025732559,21.5143777294443,-72.5494880068759));
#72834=CARTESIAN_POINT('Ctrl Pts',(-19.9209186544747,25.432709765515,-72.3506010955013));
#72835=CARTESIAN_POINT('Ctrl Pts',(-23.1721856084992,27.6212182579661,-72.1517141841263));
#72836=CARTESIAN_POINT('Ctrl Pts',(-26.7708636095538,26.0688570314354,-71.9528272727514));
#72837=CARTESIAN_POINT('Ctrl Pts',(-27.4100733050024,22.202110423209,-71.7539403613766));
#72838=CARTESIAN_POINT('Ctrl Pts',(-24.502434856255,19.5741928446358,-71.5550534500015));
#72839=CARTESIAN_POINT('Ctrl Pts',(-20.7198216424902,20.5999366146469,-71.3561665386268));
#72840=CARTESIAN_POINT('Ctrl Pts',(-19.5381344034245,24.3367707731949,-71.1572796272518));
#72841=CARTESIAN_POINT('Ctrl Pts',(-22.0432435694086,27.3508612442913,-70.9583927158769));
#72842=CARTESIAN_POINT('Ctrl Pts',(-25.9331661896048,26.8725146048559,-70.7595058045021));
#72843=CARTESIAN_POINT('Ctrl Pts',(-27.6333932006229,23.3412907709111,-70.5606188931271));
#72844=CARTESIAN_POINT('Ctrl Pts',(-25.581560127655,20.0020850943206,-70.3617319817523));
#72845=CARTESIAN_POINT('Ctrl Pts',(-21.6631276017948,19.9233444490922,-70.1628450703774));
#72846=CARTESIAN_POINT('Ctrl Pts',(-19.4788028840082,23.1774248252328,-69.9639581590025));
#72847=CARTESIAN_POINT('Ctrl Pts',(-21.0357951908098,26.774102250624,-69.7650712476277));
#72848=CARTESIAN_POINT('Ctrl Pts',(-24.9033606028634,27.4083351229759,-69.5661843362526));
#72849=CARTESIAN_POINT('Ctrl Pts',(-27.5275344222612,24.4973172047244,-69.3672974248779));
#72850=CARTESIAN_POINT('Ctrl Pts',(-26.4969234020677,20.7160271501586,-69.1684105135028));
#72851=CARTESIAN_POINT('Ctrl Pts',(-22.7585716885195,19.5391499183498,-68.9695236021282));
#72852=CARTESIAN_POINT('Ctrl Pts',(-19.7477075463674,22.0481359028861,-68.7706366907531));
#72853=CARTESIAN_POINT('Ctrl Pts',(-20.2310598430906,25.9374397107561,-68.5717497793784));
#72854=CARTESIAN_POINT('Ctrl Pts',(-23.7644687995049,27.6331209011918,-68.3728628680034));
#72855=CARTESIAN_POINT('Ctrl Pts',(-27.1010311683477,25.5769922301957,-68.1739759566284));
#72856=CARTESIAN_POINT('Ctrl Pts',(-27.1747290264866,21.6584616154734,-67.9750890452537));
#72857=CARTESIAN_POINT('Ctrl Pts',(-23.9178402908416,19.4783264553349,-67.7762021338787));
#72858=CARTESIAN_POINT('Ctrl Pts',(-20.3231695708421,21.0399461169747,-67.5773152225038));
#72859=CARTESIAN_POINT('Ctrl Pts',(-19.6939144803516,24.9083245348555,-67.3784283111289));
#72860=CARTESIAN_POINT('Ctrl Pts',(-22.6083070954968,27.5287499273489,-67.1795413997541));
#72861=CARTESIAN_POINT('Ctrl Pts',(-26.3882677027047,26.4932735341877,-66.9806544883791));
#72862=CARTESIAN_POINT('Ctrl Pts',(-27.5603329917596,22.753410366767,-66.7817675770043));
#72863=CARTESIAN_POINT('Ctrl Pts',(-25.0474743367688,19.7457775878401,-66.5828806656294));
#72864=CARTESIAN_POINT('Ctrl Pts',(-21.1587957863896,20.2341347160336,-66.3839937542544));
#72865=CARTESIAN_POINT('Ctrl Pts',(-19.4676632228503,23.769722956394,-66.1851068428796));
#72866=CARTESIAN_POINT('Ctrl Pts',(-21.5280840876475,27.1036364844786,-65.9862199315048));
#72867=CARTESIAN_POINT('Ctrl Pts',(-25.4467063009133,27.1722914372305,-65.7873330201298));
#72868=CARTESIAN_POINT('Ctrl Pts',(-27.6226482930303,23.9125997340508,-65.588446108755));
#72869=CARTESIAN_POINT('Ctrl Pts',(-26.0564038627002,20.3199416738818,-65.38955919738));
#72870=CARTESIAN_POINT('Ctrl Pts',(-22.1872188457677,19.6956654068475,-65.1906722860052));
#72871=CARTESIAN_POINT('Ctrl Pts',(-19.5705462200028,22.6134278924535,-64.9917853746302));
#72872=CARTESIAN_POINT('Ctrl Pts',(-20.6108862712309,26.392052791891,-64.7928984632553));
#72873=CARTESIAN_POINT('Ctrl Pts',(-24.3522546986636,27.5593041971357,-64.5940115518805));
#72874=CARTESIAN_POINT('Ctrl Pts',(-27.3566511332218,25.042577033367,-64.3951246405055));
#72875=CARTESIAN_POINT('Ctrl Pts',(-26.8632899823566,21.154530180813,-64.1962377291308));
#72876=CARTESIAN_POINT('Ctrl Pts',(-23.3255283135862,19.4679490449603,-63.9973508177557));
#72877=CARTESIAN_POINT('Ctrl Pts',(-19.9942691477852,21.5326586911586,-63.798463906381));
#72878=CARTESIAN_POINT('Ctrl Pts',(-19.930657214125,25.4513660130612,-63.5995769950059));
#72879=CARTESIAN_POINT('Ctrl Pts',(-23.1931464862368,27.6231112334295,-63.4006900836312));
#72880=CARTESIAN_POINT('Ctrl Pts',(-26.7837859365242,26.0522446283749,-63.2018031722561));
#72881=CARTESIAN_POINT('Ctrl Pts',(-27.4030823461947,22.1822594204177,-63.0029162608814));
#72882=CARTESIAN_POINT('Ctrl Pts',(-24.4819548224377,19.569343895035,-62.8040293495064));
#72883=CARTESIAN_POINT('Ctrl Pts',(-20.7046718888146,20.6145458813503,-62.6051424381316));
#72884=CARTESIAN_POINT('Ctrl Pts',(-19.5422363005461,24.3574133724544,-62.4062555267567));
#72885=CARTESIAN_POINT('Ctrl Pts',(-22.0628278049658,27.3585684868534,-62.2073686153818));
#72886=CARTESIAN_POINT('Ctrl Pts',(-25.9502365204291,26.8602041304068,-62.0084817040069));
#72887=CARTESIAN_POINT('Ctrl Pts',(-27.632263435331,23.3202748923593,-61.809594792632));
#72888=CARTESIAN_POINT('Ctrl Pts',(-25.563268427241,19.9916756059724,-61.6107078812572));
#72889=CARTESIAN_POINT('Ctrl Pts',(-21.6444824867456,19.9331067967561,-61.4118209698822));
#72890=CARTESIAN_POINT('Ctrl Pts',(-19.4769376349045,23.1983882345641,-61.2129340585074));
#72891=CARTESIAN_POINT('Ctrl Pts',(-21.0524238130624,26.787003128262,-61.0140471471324));
#72892=CARTESIAN_POINT('Ctrl Pts',(-24.923202802692,27.4013186549087,-60.8151602357575));
#72893=CARTESIAN_POINT('Ctrl Pts',(-27.5323569002611,24.4768309308833,-60.6162733243827));
#72894=CARTESIAN_POINT('Ctrl Pts',(-26.4822947098904,20.7008962188961,-60.4173864130077));
#72895=CARTESIAN_POINT('Ctrl Pts',(-22.7379343539384,19.5432783727942,-60.2184995016329));
#72896=CARTESIAN_POINT('Ctrl Pts',(-19.7400255301204,22.0677300433379,-60.019612590258));
#72897=CARTESIAN_POINT('Ctrl Pts',(-20.243392266773,25.9544941835025,-59.8207256788831));
#72898=CARTESIAN_POINT('Ctrl Pts',(-23.7854832113739,27.6319640917314,-59.6218387675081));
#72899=CARTESIAN_POINT('Ctrl Pts',(-27.1114171056218,25.5586871483564,-59.4229518561334));
#72900=CARTESIAN_POINT('Ctrl Pts',(-27.1649426933942,21.6398290794425,-59.2240649447584));
#72901=CARTESIAN_POINT('Ctrl Pts',(-23.8968744977499,19.4764881859506,-59.0251780333836));
#72902=CARTESIAN_POINT('Ctrl Pts',(-20.3102901039966,21.0565913279393,-58.8262911220085));
#72903=CARTESIAN_POINT('Ctrl Pts',(-19.7009564777843,24.9281576885748,-58.6274042106338));
#72904=CARTESIAN_POINT('Ctrl Pts',(-22.6287995586302,27.5335460371286,-58.4285172992588));
#72905=CARTESIAN_POINT('Ctrl Pts',(-26.4033797953935,26.4786253817834,-58.229630387884));
#72906=CARTESIAN_POINT('Ctrl Pts',(-27.5561779821169,22.7327783622798,-58.030743476509));
#72907=CARTESIAN_POINT('Ctrl Pts',(-25.0278703263696,19.7381207940882,-57.8318565651343));
#72908=CARTESIAN_POINT('Ctrl Pts',(-21.1417571986447,20.2464890772859,-57.6329696537593));
#72909=CARTESIAN_POINT('Ctrl Pts',(-19.4688470752633,23.7907358621368,-57.4340827423844));
#72910=CARTESIAN_POINT('Ctrl Pts',(-21.546402520225,27.1139988559349,-57.2351958310095));
#72911=CARTESIAN_POINT('Ctrl Pts',(-25.4653262272634,27.1624811336161,-57.0363089196346));
#72912=CARTESIAN_POINT('Ctrl Pts',(-27.6244595795468,23.8916315926108,-56.8374220082598));
#72913=CARTESIAN_POINT('Ctrl Pts',(-26.0397420906462,20.3070836387943,-56.6385350968848));
#72914=CARTESIAN_POINT('Ctrl Pts',(-22.1673947709755,19.7027329221764,-56.43964818551));
#72915=CARTESIAN_POINT('Ctrl Pts',(-19.5657764864021,22.633926510838,-56.240761274135));
#72916=CARTESIAN_POINT('Ctrl Pts',(-20.6255538595941,26.4071460210318,-56.0418743627602));
#72917=CARTESIAN_POINT('Ctrl Pts',(-24.3728813388913,27.5551226391475,-55.8429874513852));
#72918=CARTESIAN_POINT('Ctrl Pts',(-27.3642826917954,25.022963185503,-55.6441005400104));
#72919=CARTESIAN_POINT('Ctrl Pts',(-26.8509137039966,21.1375075062804,-55.4452136286355));
#72920=CARTESIAN_POINT('Ctrl Pts',(-23.3045169487698,19.4691599383696,-55.2463267172607));
#72921=CARTESIAN_POINT('Ctrl Pts',(-19.9839303593089,21.5509904441336,-55.0474398058857));
#72922=CARTESIAN_POINT('Ctrl Pts',(-19.9404914720138,25.4699732988941,-54.8485528945108));
#72923=CARTESIAN_POINT('Ctrl Pts',(-23.2141169412984,27.6248955340777,-54.649665983136));
#72924=CARTESIAN_POINT('Ctrl Pts',(-26.7966225185585,26.0355663228262,-54.450779071761));
#72925=CARTESIAN_POINT('Ctrl Pts',(-27.3959893246748,22.1624444573844,-54.2518921603862));
#72926=CARTESIAN_POINT('Ctrl Pts',(-24.4614500827513,19.5646005455128,-54.0530052490112));
#72927=CARTESIAN_POINT('Ctrl Pts',(-20.6895975482185,20.6292328813803,-53.8541183376364));
#72928=CARTESIAN_POINT('Ctrl Pts',(-19.5464443999544,24.3780346142614,-53.6552314262614));
#72929=CARTESIAN_POINT('Ctrl Pts',(-22.0824514578106,27.3661747976098,-53.4563445148867));
#72930=CARTESIAN_POINT('Ctrl Pts',(-25.9672432535572,26.8478059554361,-53.2574576035116));
#72931=CARTESIAN_POINT('Ctrl Pts',(-27.6310255029309,23.2992651032679,-53.0585706921369));
#72932=CARTESIAN_POINT('Ctrl Pts',(-25.5449233842291,19.9813604175989,-52.8596837807619));
#72933=CARTESIAN_POINT('Ctrl Pts',(-21.6258878722466,19.9429649926319,-52.660796869387));
#72934=CARTESIAN_POINT('Ctrl Pts',(-19.4751803230796,23.2193609685167,-52.4619099580122));
#72935=CARTESIAN_POINT('Ctrl Pts',(-21.0691186244834,26.7998182359834,-52.2630230466372));
#72936=CARTESIAN_POINT('Ctrl Pts',(-24.9430086211493,27.3942001389451,-52.0641361352625));
#72937=CARTESIAN_POINT('Ctrl Pts',(-27.5370738578491,24.4563201038546,-51.8652492238873));
#72938=CARTESIAN_POINT('Ctrl Pts',(-26.4675883225176,20.6858407918102,-51.6663623125127));
#72939=CARTESIAN_POINT('Ctrl Pts',(-22.7173185447046,19.5475130066537,-51.4674754011376));
#72940=CARTESIAN_POINT('Ctrl Pts',(-19.732444479779,22.0873634686633,-51.2685884897629));
#72941=CARTESIAN_POINT('Ctrl Pts',(-20.2558123178206,25.9714849470598,-51.0697015783878));
#72942=CARTESIAN_POINT('Ctrl Pts',(-23.8064913899446,27.6306991223907,-50.8708146670131));
#72943=CARTESIAN_POINT('Ctrl Pts',(-27.1217086768087,25.5403288456899,-50.6719277556381));
#72944=CARTESIAN_POINT('Ctrl Pts',(-27.1550605758581,21.6212471670735,-50.4730408442632));
#72945=CARTESIAN_POINT('Ctrl Pts',(-23.8758995196408,19.4747578658597,-50.2741539328884));
#72946=CARTESIAN_POINT('Ctrl Pts',(-20.2974964918121,21.0733026175832,-50.0752670215135));
#72947=CARTESIAN_POINT('Ctrl Pts',(-19.7081004764024,24.9479543296544,-49.8763801101385));
#72948=CARTESIAN_POINT('Ctrl Pts',(-22.6493164390321,27.5382365949702,-49.6774931987637));
#72949=CARTESIAN_POINT('Ctrl Pts',(-26.4184162840345,26.4638996314242,-49.4786062873887));
#72950=CARTESIAN_POINT('Ctrl Pts',(-27.5519168208199,22.7121680197622,-49.2797193760139));
#72951=CARTESIAN_POINT('Ctrl Pts',(-25.0082271610796,19.730565016717,-49.0808324646389));
#72952=CARTESIAN_POINT('Ctrl Pts',(-21.1247824327975,20.258930983841,-48.8819455532642));
#72953=CARTESIAN_POINT('Ctrl Pts',(-19.4701390794497,23.8117423953937,-48.6830586418892));
#72954=CARTESIAN_POINT('Ctrl Pts',(-21.5647740521415,27.1242667928908,-48.4841717305144));
#72955=CARTESIAN_POINT('Ctrl Pts',(-25.4838954067279,27.1525751107861,-48.2852848191394));
#72956=CARTESIAN_POINT('Ctrl Pts',(-27.6261629050381,23.8706544050833,-48.0863979077646));
#72957=CARTESIAN_POINT('Ctrl Pts',(-26.023014350456,20.294311543335,-47.8875109963896));
#72958=CARTESIAN_POINT('Ctrl Pts',(-22.1476073400601,19.709902391617,-47.6886240850148));
#72959=CARTESIAN_POINT('Ctrl Pts',(-19.5611123360753,22.6544494106336,-47.4897371736399));
#72960=CARTESIAN_POINT('Ctrl Pts',(-20.6402989485513,26.422163546325,-47.290850262265));
#72961=CARTESIAN_POINT('Ctrl Pts',(-24.3934861805585,27.5508349574702,-47.0919633508901));
#72962=CARTESIAN_POINT('Ctrl Pts',(-27.3718131836827,25.003310312781,-46.8930764395152));
#72963=CARTESIAN_POINT('Ctrl Pts',(-26.8384499625401,21.1205487662565,-46.6941895281402));
#72964=CARTESIAN_POINT('Ctrl Pts',(-23.283512095617,19.4704789752617,-46.4953026167655));
#72965=CARTESIAN_POINT('Ctrl Pts',(-19.9736860735894,21.5693751748738,-46.2964157053904));
#72966=CARTESIAN_POINT('Ctrl Pts',(-19.9504213837315,25.4885297147003,-46.0975287940157));
#72967=CARTESIAN_POINT('Ctrl Pts',(-23.2350963035024,27.6265718621486,-45.8986418826407));
#72968=CARTESIAN_POINT('Ctrl Pts',(-26.8093730761399,26.0188221597938,-45.6997549712659));
#72969=CARTESIAN_POINT('Ctrl Pts',(-27.3887943962852,22.1426662694047,-45.500868059891));
#72970=CARTESIAN_POINT('Ctrl Pts',(-24.4409211975515,19.5599628104253,-45.3019811485161));
#72971=CARTESIAN_POINT('Ctrl Pts',(-20.6745990111445,20.6439972845154,-45.1030942371412));
#72972=CARTESIAN_POINT('Ctrl Pts',(-19.5507585949113,24.3986339209527,-44.9042073257663));
#72973=CARTESIAN_POINT('Ctrl Pts',(-22.1021140054161,27.3736799915414,-44.7053204143916));
#72974=CARTESIAN_POINT('Ctrl Pts',(-25.9841859396713,26.8353203997202,-44.5064335030164));
#72975=CARTESIAN_POINT('Ctrl Pts',(-27.6296794355174,23.278261965007,-44.3075465916417));
#72976=CARTESIAN_POINT('Ctrl Pts',(-25.5265254851134,19.9711398000821,-44.1086596802667));
#72977=CARTESIAN_POINT('Ctrl Pts',(-21.6073442508314,19.9529187767919,-43.9097727688919));
#72978=CARTESIAN_POINT('Ctrl Pts',(-19.4735309952058,23.240342470652,-43.710885857517));
#72979=CARTESIAN_POINT('Ctrl Pts',(-21.0858791826267,26.8125472345698,-43.511998946142));
#72980=CARTESIAN_POINT('Ctrl Pts',(-24.9627775334374,27.3869797635227,-43.3131120347672));
#72981=CARTESIAN_POINT('Ctrl Pts',(-27.5416851700163,24.4357852672497,-43.1142251233922));
#72982=CARTESIAN_POINT('Ctrl Pts',(-26.4528046296572,20.6708612677958,-42.9153382120174));
#72983=CARTESIAN_POINT('Ctrl Pts',(-22.6967248071047,19.5518537077446,-42.7164513006426));
#72984=CARTESIAN_POINT('Ctrl Pts',(-19.7249645962329,22.107035658588,-42.5175643892676));
#72985=CARTESIAN_POINT('Ctrl Pts',(-20.2683196671178,25.9884115512041,-42.3186774778927));
#72986=CARTESIAN_POINT('Ctrl Pts',(-23.827492778529,27.6293260266853,-42.1197905665179));
#72987=CARTESIAN_POINT('Ctrl Pts',(-27.1319056091957,25.5219178086689,-41.9209036551429));
#72988=CARTESIAN_POINT('Ctrl Pts',(-27.1450829357411,21.6027163707607,-41.7220167437681));
#72989=CARTESIAN_POINT('Ctrl Pts',(-23.8549159123231,19.473135540914,-41.5231298323931));
#72990=CARTESIAN_POINT('Ctrl Pts',(-20.2847890733021,21.0900795430794,-41.3242429210183));
#72991=CARTESIAN_POINT('Ctrl Pts',(-19.7153462868994,24.9677139335101,-41.1253560096434));
#72992=CARTESIAN_POINT('Ctrl Pts',(-22.6698571930328,27.5428214765801,-40.9264690982685));
#72993=CARTESIAN_POINT('Ctrl Pts',(-26.4333767701808,26.4490966733227,-40.7275821868936));
#72994=CARTESIAN_POINT('Ctrl Pts',(-27.5475496207836,22.6915798853607,-40.5286952755187));
#72995=CARTESIAN_POINT('Ctrl Pts',(-24.9885453614165,19.7231104559445,-40.3298083641438));
#72996=CARTESIAN_POINT('Ctrl Pts',(-21.1078719386565,20.271460106005,-40.130921452769));
#72997=CARTESIAN_POINT('Ctrl Pts',(-19.471539201173,23.8327419995197,-39.932034541394));
#72998=CARTESIAN_POINT('Ctrl Pts',(-21.5831981965761,27.1344400232601,-39.7331476300192));
#72999=CARTESIAN_POINT('Ctrl Pts',(-25.5024133472483,27.1425736312368,-39.5342607186442));
#73000=CARTESIAN_POINT('Ctrl Pts',(-27.6277582243685,23.8496687273357,-39.3353738072694));
#73001=CARTESIAN_POINT('Ctrl Pts',(-26.0062210853925,20.281625725947,-39.1364868958945));
#73002=CARTESIAN_POINT('Ctrl Pts',(-22.127857077362,19.7171736251884,-38.9375999845196));
#73003=CARTESIAN_POINT('Ctrl Pts',(-19.556553892616,22.6749960480111,-38.7387130731447));
#73004=CARTESIAN_POINT('Ctrl Pts',(-20.6551211473777,26.4371049698264,-38.5398261617698));
#73005=CARTESIAN_POINT('Ctrl Pts',(-24.4140686776643,27.5464412657212,-38.340939250395));
#73006=CARTESIAN_POINT('Ctrl Pts',(-27.3792424093357,24.9836189359757,-38.14205233902));
#73007=CARTESIAN_POINT('Ctrl Pts',(-26.8258990882597,21.1036544101253,-37.9431654276452));
#73008=CARTESIAN_POINT('Ctrl Pts',(-23.2625143107282,19.471906120684,-37.7442785162702));
#73009=CARTESIAN_POINT('Ctrl Pts',(-19.9635365620865,21.5878123962085,-37.5453916048954));
#73010=CARTESIAN_POINT('Ctrl Pts',(-19.960446686149,25.5070347687594,-37.3465046935204));
#73011=CARTESIAN_POINT('Ctrl Pts',(-23.2560840169241,27.6281401732216,-37.1476177821456));
#73012=CARTESIAN_POINT('Ctrl Pts',(-26.8220372713958,26.0020125829756,-36.9487308707706));
#73013=CARTESIAN_POINT('Ctrl Pts',(-27.3814977516819,22.122925380574,-36.7498439593958));
#73014=CARTESIAN_POINT('Ctrl Pts',(-24.4203687108259,19.5554308126663,-36.5509570480209));
#73015=CARTESIAN_POINT('Ctrl Pts',(-20.6596766750338,20.6588386995185,-36.3520701366461));
#73016=CARTESIAN_POINT('Ctrl Pts',(-19.5551787710958,24.4192107466747,-36.1531832252711));
#73017=CARTESIAN_POINT('Ctrl Pts',(-22.1218149267513,27.3810838697706,-35.9542963138963));
#73018=CARTESIAN_POINT('Ctrl Pts',(-26.0010641298127,26.8227477941097,-35.7554094025213));
#73019=CARTESIAN_POINT('Ctrl Pts',(-27.6282252687597,23.2572660341312,-35.5565224911465));
#73020=CARTESIAN_POINT('Ctrl Pts',(-25.5080752174138,19.9610140242549,-35.3576355797715));
#73021=CARTESIAN_POINT('Ctrl Pts',(-21.5888521138813,19.9629678854739,-35.1587486683967));
#73022=CARTESIAN_POINT('Ctrl Pts',(-19.4719896949873,23.2613321849885,-34.9598617570218));
#73023=CARTESIAN_POINT('Ctrl Pts',(-21.1027050433604,26.8251897867199,-34.7609748456469));
#73024=CARTESIAN_POINT('Ctrl Pts',(-24.9825090157064,27.3796577199719,-34.562087934272));
#73025=CARTESIAN_POINT('Ctrl Pts',(-27.5461907145694,24.4152269652145,-34.3632010228971));
#73026=CARTESIAN_POINT('Ctrl Pts',(-26.4379440230572,20.6559580437898,-34.1643141115222));
#73027=CARTESIAN_POINT('Ctrl Pts',(-22.6761536868454,19.5563003610444,-33.9654272001473));
#73028=CARTESIAN_POINT('Ctrl Pts',(-19.7175860776892,22.126746091825,-33.7665402887725));
#73029=CARTESIAN_POINT('Ctrl Pts',(-20.2809139832361,26.0052735474027,-33.5676533773975));
#73030=CARTESIAN_POINT('Ctrl Pts',(-23.8484868206187,27.6278448410005,-33.3687664660227));
#73031=CARTESIAN_POINT('Ctrl Pts',(-27.1420076325773,25.5034545251612,-33.1698795546478));
#73032=CARTESIAN_POINT('Ctrl Pts',(-27.1350100374375,21.5842371815452,-32.9709926432729));
#73033=CARTESIAN_POINT('Ctrl Pts',(-23.8339242318343,19.4716212541032,-32.7721057318979));
#73034=CARTESIAN_POINT('Ctrl Pts',(-20.2721681851962,21.1069216598618,-32.5732188205231));
#73035=CARTESIAN_POINT('Ctrl Pts',(-19.7226937172709,24.9874359765389,-32.3743319091482));
#73036=CARTESIAN_POINT('Ctrl Pts',(-22.6904212763297,27.5473005604653,-32.1754449977733));
#73037=CARTESIAN_POINT('Ctrl Pts',(-26.4482608574,26.4342168997375,-31.9765580863984));
#73038=CARTESIAN_POINT('Ctrl Pts',(-27.543076497733,22.6710145046333,-31.7776711750235));
#73039=CARTESIAN_POINT('Ctrl Pts',(-24.9688254489214,19.7157573093065,-31.5787842636486));
#73040=CARTESIAN_POINT('Ctrl Pts',(-21.091026164327,20.2840761117728,-31.3798973522737));
#73041=CARTESIAN_POINT('Ctrl Pts',(-19.4730474033318,23.8537341180536,-31.1810104408989));
#73042=CARTESIAN_POINT('Ctrl Pts',(-21.6016744653136,27.1445182774654,-30.9821235295239));
#73043=CARTESIAN_POINT('Ctrl Pts',(-25.520879558124,27.1324769599941,-30.7832366181491));
#73044=CARTESIAN_POINT('Ctrl Pts',(-27.629245495264,23.8286751154602,-30.5843497067742));
#73045=CARTESIAN_POINT('Ctrl Pts',(-25.9893627404548,20.2690265227877,-30.3854627953993));
#73046=CARTESIAN_POINT('Ctrl Pts',(-22.1081445062367,19.7245464302124,-30.1865758840244));
#73047=CARTESIAN_POINT('Ctrl Pts',(-19.552101276817,22.6955658785119,-29.9876889726495));
#73048=CARTESIAN_POINT('Ctrl Pts',(-20.6700200633047,26.4519698956079,-29.7888020612746));
#73049=CARTESIAN_POINT('Ctrl Pts',(-24.4346282848001,27.5419416803281,-29.5899151498998));
#73050=CARTESIAN_POINT('Ctrl Pts',(-27.3865701718898,24.9638895768821,-29.3910282385248));
#73051=CARTESIAN_POINT('Ctrl Pts',(-26.8132614137367,21.0868248855645,-29.19214132715));
#73052=CARTESIAN_POINT('Ctrl Pts',(-23.2415241505165,19.473441336819,-28.993254415775));
#73053=CARTESIAN_POINT('Ctrl Pts',(-19.9534820937486,21.606301619576,-28.7943675044002));
#73054=CARTESIAN_POINT('Ctrl Pts',(-19.970567113609,25.5254879707124,-28.5954805930253));
#73055=CARTESIAN_POINT('Ctrl Pts',(-23.2770795254171,27.6296004257387,-28.3965936816504));
#73056=CARTESIAN_POINT('Ctrl Pts',(-26.8346147687422,25.9851380378026,-28.1977067702755));
#73057=CARTESIAN_POINT('Ctrl Pts',(-27.3740995842164,22.1032223139994,-27.9988198589006));
#73058=CARTESIAN_POINT('Ctrl Pts',(-24.399793167188,19.5510046723275,-27.7999329475257));
#73059=CARTESIAN_POINT('Ctrl Pts',(-20.6448309353086,20.6737567331121,-27.6010460361508));
#73060=CARTESIAN_POINT('Ctrl Pts',(-19.5597048113794,24.4397645461687,-27.4021591247759));
#73061=CARTESIAN_POINT('Ctrl Pts',(-22.1415536997682,27.388386236105,-27.2032722134011));
#73062=CARTESIAN_POINT('Ctrl Pts',(-26.0178773767323,26.8100884717615,-27.0043853020261));
#73063=CARTESIAN_POINT('Ctrl Pts',(-27.6266630411912,23.2362778670052,-26.8054983906513));
#73064=CARTESIAN_POINT('Ctrl Pts',(-25.4895730700376,19.9509833584364,-26.6066114792763));
#73065=CARTESIAN_POINT('Ctrl Pts',(-21.5704119514127,19.9731120523902,-26.4077245679015));
#73066=CARTESIAN_POINT('Ctrl Pts',(-19.4705564632671,23.2823295553269,-26.2088376565266));
#73067=CARTESIAN_POINT('Ctrl Pts',(-21.1195957608214,26.8377455574228,-26.0099507451517));
#73068=CARTESIAN_POINT('Ctrl Pts',(-25.0022025450986,27.3722342023172,-25.8110638337769));
#73069=CARTESIAN_POINT('Ctrl Pts',(-27.5505903721173,24.3946457425163,-25.6121769224019));
#73070=CARTESIAN_POINT('Ctrl Pts',(-26.4230068965039,20.6411315147079,-25.4132900110271));
#73071=CARTESIAN_POINT('Ctrl Pts',(-22.6556057290338,19.5608528487226,-25.2144030996521));
#73072=CARTESIAN_POINT('Ctrl Pts',(-19.7103091196687,22.1464942460744,-25.0155161882773));
#73073=CARTESIAN_POINT('Ctrl Pts',(-20.2935949324433,26.0220704888353,-24.8166292769023));
#73074=CARTESIAN_POINT('Ctrl Pts',(-23.8694729598992,27.6262556045857,-24.6177423655275));
#73075=CARTESIAN_POINT('Ctrl Pts',(-27.1520144792637,25.4849394844189,-24.4188554541526));
#73076=CARTESIAN_POINT('Ctrl Pts',(-27.1248421478655,21.5658100891014,-24.2199685427777));
#73077=CARTESIAN_POINT('Ctrl Pts',(-23.8129250344257,19.4702150455535,-24.0210816314028));
#73078=CARTESIAN_POINT('Ctrl Pts',(-20.2596341619313,21.1238285216369,-23.822194720028));
#73079=CARTESIAN_POINT('Ctrl Pts',(-19.7301425728201,25.0071199361328,-23.623307808653));
#73080=CARTESIAN_POINT('Ctrl Pts',(-22.7110081440022,27.5516737279358,-23.4244208972782));
#73081=CARTESIAN_POINT('Ctrl Pts',(-26.4630681512832,26.4192607049628,-23.2255339859032));
#73082=CARTESIAN_POINT('Ctrl Pts',(-27.5384975701998,22.6504724225348,-23.0266470745284));
#73083=CARTESIAN_POINT('Ctrl Pts',(-24.9490679461458,19.7085057716518,-22.8277601631535));
#73084=CARTESIAN_POINT('Ctrl Pts',(-21.0742455561998,20.2967786668372,-22.6288732517786));
#73085=CARTESIAN_POINT('Ctrl Pts',(-19.4746636459607,23.8747181947322,-22.4299863404037));
#73086=CARTESIAN_POINT('Ctrl Pts',(-21.6202023687578,27.1545012884469,-22.2310994290288));
#73087=CARTESIAN_POINT('Ctrl Pts',(-25.5392935500252,27.1222853646061,-22.0322125176539));
#73088=CARTESIAN_POINT('Ctrl Pts',(-27.6306246783143,23.8076741257598,-21.833325606279));
#73089=CARTESIAN_POINT('Ctrl Pts',(-25.9724397623662,20.256514267719,-21.6344386949041));
#73090=CARTESIAN_POINT('Ctrl Pts',(-22.0884701490409,19.7320206113193,-21.4355517835292));
#73091=CARTESIAN_POINT('Ctrl Pts',(-19.5477546066665,22.7161583570634,-21.2366648721544));
#73092=CARTESIAN_POINT('Ctrl Pts',(-20.6849953015308,26.4667579297692,-21.0377779607794));
#73093=CARTESIAN_POINT('Ctrl Pts',(-24.4551644571639,27.5373363205236,-20.8388910494046));
#73094=CARTESIAN_POINT('Ctrl Pts',(-27.3937962771691,24.9441227583021,-20.6400041380297));
#73095=CARTESIAN_POINT('Ctrl Pts',(-26.8005372738526,21.0700606385341,-20.4411172266548));
#73096=CARTESIAN_POINT('Ctrl Pts',(-23.2205421711933,19.4750845829856,-20.2422303152799));
#73097=CARTESIAN_POINT('Ctrl Pts',(-19.9435229350058,21.6248423550366,-20.043343403905));
#73098=CARTESIAN_POINT('Ctrl Pts',(-19.980782397934,25.543888831574,-19.8444564925301));
#73099=CARTESIAN_POINT('Ctrl Pts',(-23.2980822726284,27.6309525810051,-19.6455695811552));
#73100=CARTESIAN_POINT('Ctrl Pts',(-26.8471052348921,25.9681989714279,-19.4466826697803));
#73101=CARTESIAN_POINT('Ctrl Pts',(-27.3666000899299,22.0835575917858,-19.2477957584055));
#73102=CARTESIAN_POINT('Ctrl Pts',(-24.3791951118623,19.5466845066959,-19.0489088470305));
#73103=CARTESIAN_POINT('Ctrl Pts',(-20.6300621853608,20.6887509899882,-18.8500219356557));
#73104=CARTESIAN_POINT('Ctrl Pts',(-19.5643365958281,24.4602947747868,-18.6511350242807));
#73105=CARTESIAN_POINT('Ctrl Pts',(-22.1613298014156,27.3955868970413,-18.4522481129059));
#73106=CARTESIAN_POINT('Ctrl Pts',(-26.0346252349013,26.797342768131,-18.253361201531));
#73107=CARTESIAN_POINT('Ctrl Pts',(-27.6249927942088,23.2152980197868,-18.0544742901561));
#73108=CARTESIAN_POINT('Ctrl Pts',(-25.4710195332669,19.9410480684262,-17.8555873787812));
#73109=CARTESIAN_POINT('Ctrl Pts',(-21.5520242520656,19.9833510087338,-17.6567004674063));
#73110=CARTESIAN_POINT('Ctrl Pts',(-19.4692313380238,23.3033340252649,-17.4578135560314));
#73111=CARTESIAN_POINT('Ctrl Pts',(-21.1365508874283,26.8502142139675,-17.2589266446566));
#73112=CARTESIAN_POINT('Ctrl Pts',(-25.0218575997618,27.3647094072718,-17.0600397332816));
#73113=CARTESIAN_POINT('Ctrl Pts',(-27.5548840260751,24.37404214453,-16.8611528219068));
#73114=CARTESIAN_POINT('Ctrl Pts',(-26.4079936458107,20.6263820734331,-16.6622659105319));
#73115=CARTESIAN_POINT('Ctrl Pts',(-22.6350814781631,19.5655110501445,-16.463378999157));
#73116=CARTESIAN_POINT('Ctrl Pts',(-19.703133915001,22.1662795980365,-16.2644920877821));
#73117=CARTESIAN_POINT('Ctrl Pts',(-20.3063621787112,26.0388019304058,-16.0656051764072));
#73118=CARTESIAN_POINT('Ctrl Pts',(-23.8904506402666,27.6245583595535,-15.8667182650323));
#73119=CARTESIAN_POINT('Ctrl Pts',(-27.1619258840868,25.4663731770661,-15.6678313536574));
#73120=CARTESIAN_POINT('Ctrl Pts',(-27.1145795364606,21.5474355817217,-15.4689444422825));
#73121=CARTESIAN_POINT('Ctrl Pts',(-23.7919188765479,19.4689169525278,-15.2700575309077));
#73122=CARTESIAN_POINT('Ctrl Pts',(-20.2471873356418,21.1407996803954,-15.0711706195327));
#73123=CARTESIAN_POINT('Ctrl Pts',(-19.7376926561622,25.0267652906936,-14.8722837081579));
#73124=CARTESIAN_POINT('Ctrl Pts',(-22.7316172505259,27.5559408631087,-14.673396796783));
#73125=CARTESIAN_POINT('Ctrl Pts',(-26.4777982594575,26.4042284853174,-14.4745098854081));
#73126=CARTESIAN_POINT('Ctrl Pts',(-27.5338129595197,22.6299541834031,-14.2756229740332));
#73127=CARTESIAN_POINT('Ctrl Pts',(-24.9292733766367,19.701356035136,-14.0767360626583));
#73128=CARTESIAN_POINT('Ctrl Pts',(-21.057530558938,20.3095674345978,-13.8778491512834));
#73129=CARTESIAN_POINT('Ctrl Pts',(-19.4763878862318,23.8956936735058,-13.6789622399085));
#73130=CARTESIAN_POINT('Ctrl Pts',(-21.6387814159439,27.1643887916678,-13.4800753285336));
#73131=CARTESIAN_POINT('Ctrl Pts',(-25.5576548350058,27.1119991151366,-13.2811884171587));
#73132=CARTESIAN_POINT('Ctrl Pts',(-27.6318957369723,23.786666314732,-13.0823015057838));
#73133=CARTESIAN_POINT('Ctrl Pts',(-25.955452599563,20.2440892922991,-12.8834145944089));
#73134=CARTESIAN_POINT('Ctrl Pts',(-22.0688345271186,19.7395959704539,-12.6845276830341));
#73135=CARTESIAN_POINT('Ctrl Pts',(-19.5435139973455,22.7367729379924,-12.4856407716592));
#73136=CARTESIAN_POINT('Ctrl Pts',(-20.7000464652327,26.4814686804472,-12.2867538602843));
#73137=CARTESIAN_POINT('Ctrl Pts',(-24.4756766505751,27.5326253083435,-12.0878669489094));
#73138=CARTESIAN_POINT('Ctrl Pts',(-27.4009205336917,24.9243190040294,-11.8889800375345));
#73139=CARTESIAN_POINT('Ctrl Pts',(-26.7877270057798,21.053362113264,-11.6900931261596));
#73140=CARTESIAN_POINT('Ctrl Pts',(-23.1995689287524,19.4768358156397,-11.4912062147847));
#73141=CARTESIAN_POINT('Ctrl Pts',(-19.9336593497623,21.6434341112861,-11.2923193034098));
#73142=CARTESIAN_POINT('Ctrl Pts',(-19.9910922684325,25.5622368637462,-11.0934323920349));
#73143=CARTESIAN_POINT('Ctrl Pts',(-23.3190917020137,27.6321966031907,-10.8945454806601));
#73144=CARTESIAN_POINT('Ctrl Pts',(-26.8595083388649,25.9511958327137,-10.6956585692851));
#73145=CARTESIAN_POINT('Ctrl Pts',(-27.3589994675491,22.0639317350221,-10.4967716579103));
#73146=CARTESIAN_POINT('Ctrl Pts',(-24.3585750906692,19.54247043025,-10.2978847465354));
#73147=CARTESIAN_POINT('Ctrl Pts',(-20.6153708165425,20.7038210728193,-10.0989978351605));
#73148=CARTESIAN_POINT('Ctrl Pts',(-19.5690740017059,24.4808008885054,-9.90011092378563));
#73149=CARTESIAN_POINT('Ctrl Pts',(-22.1811427076536,27.4026856617719,-9.70122401241075));
#73150=CARTESIAN_POINT('Ctrl Pts',(-26.0513072605242,26.784511020962,-9.50233710103585));
#73151=CARTESIAN_POINT('Ctrl Pts',(-27.6232145720716,23.1943270484138,-9.30345018966096));
#73152=CARTESIAN_POINT('Ctrl Pts',(-25.4524150987455,19.931208417496,-9.10456327828608));
#73153=CARTESIAN_POINT('Ctrl Pts',(-21.533689503089,19.9936844831863,-8.90567636691117));
#73154=CARTESIAN_POINT('Ctrl Pts',(-19.4680143543712,23.3243450382125,-8.7067894555363));
#73155=CARTESIAN_POINT('Ctrl Pts',(-21.1535699738932,26.8625954259514,-8.50790254416139));
#73156=CARTESIAN_POINT('Ctrl Pts',(-25.0414736588636,27.3570835342327,-8.30901563278651));
#73157=CARTESIAN_POINT('Ctrl Pts',(-27.5590715626666,24.3534167172232,-8.11012872141162));
#73158=CARTESIAN_POINT('Ctrl Pts',(-26.3929046688091,20.6117101108059,-7.91124181003674));
#73159=CARTESIAN_POINT('Ctrl Pts',(-22.6145814780984,19.5702748418738,-7.71235489866183));
#73160=CARTESIAN_POINT('Ctrl Pts',(-19.6960606538194,22.1861016234263,-7.51346798728695));
#73161=CARTESIAN_POINT('Ctrl Pts',(-20.3192153837249,26.0554674287532,-7.31458107591206));
#73162=CARTESIAN_POINT('Ctrl Pts',(-23.91141930584,27.6227531508786,-7.11569416453717));
#73163=CARTESIAN_POINT('Ctrl Pts',(-27.1717415844078,25.4477560950847,-6.91680725316227));
#73164=CARTESIAN_POINT('Ctrl Pts',(-27.104222475168,21.5291141463064,-6.71792034178739));
#73165=CARTESIAN_POINT('Ctrl Pts',(-23.770906314836,19.4677270094237,-6.51903343041249));
#73166=CARTESIAN_POINT('Ctrl Pts',(-20.2348280361521,21.1578346864247,-6.32014651903762));
#73167=CARTESIAN_POINT('Ctrl Pts',(-19.7453437672301,25.0463715196455,-6.12125960766271));
#73168=CARTESIAN_POINT('Ctrl Pts',(-22.7522480497871,27.5601018529106,-5.92237269628783));
#73169=CARTESIAN_POINT('Ctrl Pts',(-26.4924507915943,26.3891206391351,-5.72348578491294));
#73170=CARTESIAN_POINT('Ctrl Pts',(-27.5290227898282,22.609460330944,-5.52459887353805));
#73171=CARTESIAN_POINT('Ctrl Pts',(-24.909442264924,19.6943082892178,-5.32571196216315));
#73172=CARTESIAN_POINT('Ctrl Pts',(-21.040881615467,20.3224420761691,-5.12682505078827));
#73173=CARTESIAN_POINT('Ctrl Pts',(-19.4782200784547,23.9166599985522,-4.92793813941337));
#73174=CARTESIAN_POINT('Ctrl Pts',(-21.6574111145523,27.1741805251229,-4.72905122803848));
#73175=CARTESIAN_POINT('Ctrl Pts',(-25.5759629265164,27.1016184841571,-4.53016431666359));
#73176=CARTESIAN_POINT('Ctrl Pts',(-27.6330586375572,23.7656522390559,-4.33127740528871));
#73177=CARTESIAN_POINT('Ctrl Pts',(-25.9384017021823,20.2317519257727,-4.13239049391381));
#73178=CARTESIAN_POINT('Ctrl Pts',(-22.0492381607876,19.747272306879,-3.93350358253892));
#73179=CARTESIAN_POINT('Ctrl Pts',(-19.5393795612244,22.7574090750401,-3.73461667116403));
#73180=CARTESIAN_POINT('Ctrl Pts',(-20.7151731555746,26.4961017578267,-3.53572975978914));
#73181=CARTESIAN_POINT('Ctrl Pts',(-24.4961643214874,27.5278087686234,-3.33684284841425));
#73182=CARTESIAN_POINT('Ctrl Pts',(-27.4079427526743,24.9044788388371,-3.13795593703936));
#73183=CARTESIAN_POINT('Ctrl Pts',(-26.7748309489734,21.0367297522428,-2.93906902566447));
#73184=CARTESIAN_POINT('Ctrl Pts',(-23.1786049789569,19.4786949883764,-2.74018211428958));
#73185=CARTESIAN_POINT('Ctrl Pts',(-19.9238915993898,21.6620763956673,-2.54129520291469));
#73186=CARTESIAN_POINT('Ctrl Pts',(-20.0014964519067,25.580531581031,-2.34240829153979));
#73187=CARTESIAN_POINT('Ctrl Pts',(-23.340107256851,27.6333324593303,-2.14352138016491));
#73188=CARTESIAN_POINT('Ctrl Pts',(-26.871823751995,25.9341290722209,-1.94463446879002));
#73189=CARTESIAN_POINT('Ctrl Pts',(-27.3512979184802,22.0443452637667,-1.74574755741513));
#73190=CARTESIAN_POINT('Ctrl Pts',(-24.3379336500121,19.5383625546572,-1.54686064604024));
#73191=CARTESIAN_POINT('Ctrl Pts',(-20.6007572181553,20.7189665822683,-1.34797373466534));
#73192=CARTESIAN_POINT('Ctrl Pts',(-19.5739169034777,24.50128234394,-1.14908682329046));
#73193=CARTESIAN_POINT('Ctrl Pts',(-22.2009918934665,27.4096823421886,-0.95019991191556));
#73194=CARTESIAN_POINT('Ctrl Pts',(-26.0679230115496,26.7715935702787,-0.751313000540672));
#73195=CARTESIAN_POINT('Ctrl Pts',(-27.6213284219005,23.1733655085891,-0.552426089165777));
#73196=CARTESIAN_POINT('Ctrl Pts',(-25.4337602594659,19.9214646663832,-0.353539177790892));
#73197=CARTESIAN_POINT('Ctrl Pts',(-21.5154081903294,20.0041122019244,-0.154652266415998));
#73198=CARTESIAN_POINT('Ctrl Pts',(-19.466905544558,23.3453620374057,0.0442346449588902));
#73199=CARTESIAN_POINT('Ctrl Pts',(-21.170652569233,26.874888865289,0.24312155633378));
#73200=CARTESIAN_POINT('Ctrl Pts',(-25.0610502026044,27.3493567852751,0.44200846770867));
#73201=CARTESIAN_POINT('Ctrl Pts',(-27.5631528709278,24.3327700071423,0.640895379083562));
#73202=CARTESIAN_POINT('Ctrl Pts',(-26.3777403653365,20.5971160156136,0.839782290458452));
#73203=CARTESIAN_POINT('Ctrl Pts',(-22.5941062720623,19.5751440976768,1.03866920183334));
#73204=CARTESIAN_POINT('Ctrl Pts',(-19.6890895235559,22.2059597969863,1.23755611320823));
#73205=CARTESIAN_POINT('Ctrl Pts',(-20.3321542068916,26.0720665422642,1.43644302458312));
#73206=CARTESIAN_POINT('Ctrl Pts',(-23.9323784009782,27.6208400263966,1.63532993595801));
#73207=CARTESIAN_POINT('Ctrl Pts',(-27.1814613201236,25.4290887318025,1.83421684733291));
#73208=CARTESIAN_POINT('Ctrl Pts',(-27.0937712384363,21.5108462683488,2.03310375870779));
#73209=CARTESIAN_POINT('Ctrl Pts',(-23.7498879060944,19.4666452477732,2.2319906700827));
#73210=CARTESIAN_POINT('Ctrl Pts',(-20.222556590967,21.1749330883198,2.43087758145757));
#73211=CARTESIAN_POINT('Ctrl Pts',(-19.7530957032797,25.06593810345,2.62976449283247));
#73212=CARTESIAN_POINT('Ctrl Pts',(-22.7728999950974,27.564156587081,2.82865140420734));
#73213=CARTESIAN_POINT('Ctrl Pts',(-26.5070253594215,26.3739375667534,3.02753831558225));
#73214=CARTESIAN_POINT('Ctrl Pts',(-27.5241271880586,22.5889914082169,3.22642522695711));
#73215=CARTESIAN_POINT('Ctrl Pts',(-24.8895751365054,19.6873627206529,3.42531213833204));
#73216=CARTESIAN_POINT('Ctrl Pts',(-21.0242991669612,20.3354022503905,3.62419904970691));
#73217=CARTESIAN_POINT('Ctrl Pts',(-19.480160174079,23.9376166142918,3.82308596108181));
#73218=CARTESIAN_POINT('Ctrl Pts',(-21.6760909709207,27.1838762293441,4.02197287245669));
#73219=CARTESIAN_POINT('Ctrl Pts',(-25.5942173394172,27.0911437467407,4.22085978383159));
#73220=CARTESIAN_POINT('Ctrl Pts',(-27.6341133492534,23.7446324555762,4.41974669520646));
#73221=CARTESIAN_POINT('Ctrl Pts',(-25.92128752205,20.2195024950638,4.61863360658138));
#73222=CARTESIAN_POINT('Ctrl Pts',(-22.0296815693252,19.7550494171818,4.81752051795627));
#73223=CARTESIAN_POINT('Ctrl Pts',(-19.5353514078603,22.7780662213765,5.01640742933116));
#73224=CARTESIAN_POINT('Ctrl Pts',(-20.7303749717194,26.5106567741508,5.21529434070603));
#73225=CARTESIAN_POINT('Ctrl Pts',(-24.5166269270054,27.522886828995,5.41418125208093));
#73226=CARTESIAN_POINT('Ctrl Pts',(-27.4148627480375,24.8846027884633,5.61306816345578));
#73227=CARTESIAN_POINT('Ctrl Pts',(-26.7618494451617,21.0201639962057,5.81195507483073));
#73228=CARTESIAN_POINT('Ctrl Pts',(-23.1576508773234,19.4806620519298,6.01084198620561));
#73229=CARTESIAN_POINT('Ctrl Pts',(-19.9142199427209,21.6807687141851,6.2097288975805));
#73230=CARTESIAN_POINT('Ctrl Pts',(-20.0119946726599,25.5987724986425,6.40861580895537));
#73231=CARTESIAN_POINT('Ctrl Pts',(-23.3611283802564,27.6343601193255,6.60750272033028));
#73232=CARTESIAN_POINT('Ctrl Pts',(-26.8840511479407,25.9169991421951,6.80638963170513));
#73233=CARTESIAN_POINT('Ctrl Pts',(-27.3434956468041,22.0247986970354,7.00527654308008));
#73234=CARTESIAN_POINT('Ctrl Pts',(-24.3172713368611,19.5343609887707,7.20416345445494));
#73235=CARTESIAN_POINT('Ctrl Pts',(-20.58622177744,20.7341871169995,7.40305036582984));
#73236=CARTESIAN_POINT('Ctrl Pts',(-19.5788651728132,24.5217385983595,7.60193727720472));
#73237=CARTESIAN_POINT('Ctrl Pts',(-22.2208768328776,27.4165767528892,7.80082418857962));
#73238=CARTESIAN_POINT('Ctrl Pts',(-26.0844720476824,26.7585907583762,7.99971109995449));
#73239=CARTESIAN_POINT('Ctrl Pts',(-27.6193343936757,23.1524139557652,8.19859801132941));
#73240=CARTESIAN_POINT('Ctrl Pts',(-25.4150555097565,19.9118170732843,8.39748492270429));
#73241=CARTESIAN_POINT('Ctrl Pts',(-21.4971807982172,20.0146338886273,8.59637183407918));
#73242=CARTESIAN_POINT('Ctrl Pts',(-19.4659049379659,23.3663844659224,8.79525874545406));
#73243=CARTESIAN_POINT('Ctrl Pts',(-21.187798220782,26.8870942062206,8.99414565682896));
#73244=CARTESIAN_POINT('Ctrl Pts',(-25.0805867122322,27.3415293651475,9.19303256820384));
#73245=CARTESIAN_POINT('Ctrl Pts',(-27.5671278427097,24.3121025613973,9.39191947957871));
#73246=CARTESIAN_POINT('Ctrl Pts',(-26.3625011372266,20.5826001745801,9.59080639095364));
#73247=CARTESIAN_POINT('Ctrl Pts',(-22.5736564026206,19.5801186885244,9.78969330232851));
#73248=CARTESIAN_POINT('Ctrl Pts',(-19.6822207089359,22.2258535925017,9.98858021370343));
#73249=CARTESIAN_POINT('Ctrl Pts',(-20.3451783053501,26.0885988310845,10.1874671250783));
#73250=CARTESIAN_POINT('Ctrl Pts',(-23.9533273702929,27.6188190368028,10.3863540364532));
#73251=CARTESIAN_POINT('Ctrl Pts',(-27.1910848336742,25.4103715818797,10.5852409478281));
#73252=CARTESIAN_POINT('Ctrl Pts',(-27.0832261032093,21.4926324319235,10.784127859203));
#73253=CARTESIAN_POINT('Ctrl Pts',(-23.7288642072832,19.4656716962415,10.9830147705779));
#73254=CARTESIAN_POINT('Ctrl Pts',(-20.2103733252635,21.1920944329958,11.1819016819528));
#73255=CARTESIAN_POINT('Ctrl Pts',(-19.7609482588949,25.0854645236187,11.3807885933277));
#73256=CARTESIAN_POINT('Ctrl Pts',(-22.793572539208,27.5681049581747,11.5796755047026));
#73257=CARTESIAN_POINT('Ctrl Pts',(-26.5215215767324,26.3586796705037,11.7785624160775));
#73258=CARTESIAN_POINT('Ctrl Pts',(-27.5191262839377,22.5685479576211,11.9774493274523));
#73259=CARTESIAN_POINT('Ctrl Pts',(-24.8696725178331,19.6805195134897,12.1763362388272));
#73260=CARTESIAN_POINT('Ctrl Pts',(-21.0077836528336,20.3484476138346,12.3752231502021));
#73261=CARTESIAN_POINT('Ctrl Pts',(-19.4822081216946,23.9585629654026,12.5741100615771));
#73262=CARTESIAN_POINT('Ctrl Pts',(-21.6948204900581,27.1934756474084,12.7729969729519));
#73263=CARTESIAN_POINT('Ctrl Pts',(-25.6124175899905,27.0805751804539,12.9718838843268));
#73264=CARTESIAN_POINT('Ctrl Pts',(-27.6350598441126,23.7236075212892,13.1707707957017));
#73265=CARTESIAN_POINT('Ctrl Pts',(-25.9041105126688,20.207341324766,13.3696577070766));
#73266=CARTESIAN_POINT('Ctrl Pts',(-22.0101652709548,19.7629270952796,13.5685446184515));
#73267=CARTESIAN_POINT('Ctrl Pts',(-19.5314296439939,22.7987438296151,13.7674315298264));
#73268=CARTESIAN_POINT('Ctrl Pts',(-20.7456515108394,26.5251333437309,13.9663184412013));
#73269=CARTESIAN_POINT('Ctrl Pts',(-24.5370639248974,27.5178596198832,14.1652053525761));
#73270=CARTESIAN_POINT('Ctrl Pts',(-27.4216803364103,24.8646913795963,14.3640922639511));
#73271=CARTESIAN_POINT('Ctrl Pts',(-26.7487828383371,21.0036652841232,14.5629791753259));
#73272=CARTESIAN_POINT('Ctrl Pts',(-23.1367071791074,19.4827369541754,14.7618660867009));
#73273=CARTESIAN_POINT('Ctrl Pts',(-19.9046446360413,21.6995105715179,14.9607529980757));
#73274=CARTESIAN_POINT('Ctrl Pts',(-20.0225866525029,25.616959133221,15.1596399094506));
#73275=CARTESIAN_POINT('Ctrl Pts',(-23.3821545151984,27.6352795559443,15.3585268208255));
#73276=CARTESIAN_POINT('Ctrl Pts',(-26.8961902026918,25.899806496557,15.5574137322004));
#73277=CARTESIAN_POINT('Ctrl Pts',(-27.3355928592704,22.0052925527857,15.7563006435752));
#73278=CARTESIAN_POINT('Ctrl Pts',(-24.29658869874,19.5304658386265,15.9551875549502));
#73279=CARTESIAN_POINT('Ctrl Pts',(-20.5717648795662,20.7494822736892,16.154074466325));
#73280=CARTESIAN_POINT('Ctrl Pts',(-19.5839186785901,24.5421691097005,16.3529613777));
#73281=CARTESIAN_POINT('Ctrl Pts',(-22.2407969989625,27.423368711181,16.5518482890748));
#73282=CARTESIAN_POINT('Ctrl Pts',(-26.100953930395,26.7455029298116,16.7507352004497));
#73283=CARTESIAN_POINT('Ctrl Pts',(-27.6172325402363,23.1314729451304,16.9496221118246));
#73284=CARTESIAN_POINT('Ctrl Pts',(-25.3963013452681,19.9022658938477,17.1485090231995));
#73285=CARTESIAN_POINT('Ctrl Pts',(-21.4790078097535,20.0252492644848,17.3473959345744));
#73286=CARTESIAN_POINT('Ctrl Pts',(-19.4650125611099,23.3874117666964,17.5462828459493));
#73287=CARTESIAN_POINT('Ctrl Pts',(-21.2050064742031,26.899211125321,17.7451697573242));
#73288=CARTESIAN_POINT('Ctrl Pts',(-25.1000826700559,27.3336014812664,17.9440566686991));
#73289=CARTESIAN_POINT('Ctrl Pts',(-27.5709963726804,24.2914149276475,18.1429435800739));
#73290=CARTESIAN_POINT('Ctrl Pts',(-26.3471873882987,20.5681629723558,18.3418304914489));
#73291=CARTESIAN_POINT('Ctrl Pts',(-22.5532324116668,19.5851984825965,18.5407174028237));
#73292=CARTESIAN_POINT('Ctrl Pts',(-19.6754543919742,22.2457824828137,18.7396043141986));
#73293=CARTESIAN_POINT('Ctrl Pts',(-20.3582873339789,26.1050638571306,18.9384912255735));
#73294=CARTESIAN_POINT('Ctrl Pts',(-23.974265658665,27.6166902356509,19.1373781369484));
#73295=CARTESIAN_POINT('Ctrl Pts',(-27.2006118700494,25.3916051412957,19.3362650483233));
#73296=CARTESIAN_POINT('Ctrl Pts',(-27.0725873489185,21.4744731196725,19.5351519596982));
#73297=CARTESIAN_POINT('Ctrl Pts',(-23.7078357755019,19.4648063806263,19.7340388710731));
#73298=CARTESIAN_POINT('Ctrl Pts',(-20.1982785618818,21.2093182657003,19.932925782448));
#73299=CARTESIAN_POINT('Ctrl Pts',(-19.7689012259936,25.1049502627275,20.1318126938229));
#73300=CARTESIAN_POINT('Ctrl Pts',(-22.8142651343239,27.5719468615651,20.3306996051977));
#73301=CARTESIAN_POINT('Ctrl Pts',(-26.5359390593967,26.3433473546996,20.5295865165726));
#73302=CARTESIAN_POINT('Ctrl Pts',(-27.5140202099829,22.5481305208802,20.7284734279475));
#73303=CARTESIAN_POINT('Ctrl Pts',(-24.8497349363,19.6737788490641,20.9273603393224));
#73304=CARTESIAN_POINT('Ctrl Pts',(-20.991335510723,20.3615778208169,21.1262472506973));
#73305=CARTESIAN_POINT('Ctrl Pts',(-19.4843638670336,23.9794984968342,21.3251341620722));
#73306=CARTESIAN_POINT('Ctrl Pts',(-21.7135991756574,27.202978524944,21.5240210734471));
#73307=CARTESIAN_POINT('Ctrl Pts',(-25.6305631959542,27.0699130653494,21.722907984822));
#73308=CARTESIAN_POINT('Ctrl Pts',(-27.6358980970538,23.7025779933274,21.9217948961968));
#73309=CARTESIAN_POINT('Ctrl Pts',(-25.8868711292066,20.1952687371338,22.1206818075718));
#73310=CARTESIAN_POINT('Ctrl Pts',(-21.9906897828324,19.7709051324244,22.3195687189467));
#73311=CARTESIAN_POINT('Ctrl Pts',(-19.5276143735466,22.8194413518271,22.5184556303215));
#73312=CARTESIAN_POINT('Ctrl Pts',(-20.7610023681266,26.5395310829572,22.7173425416964));
#73313=CARTESIAN_POINT('Ctrl Pts',(-24.5574747736107,27.5127272745031,22.9162294530713));
#73314=CARTESIAN_POINT('Ctrl Pts',(-27.428395337136,24.8447451398607,23.1151163644462));
#73315=CARTESIAN_POINT('Ctrl Pts',(-26.7356314747477,20.9872340531911,23.3140032758211));
#73316=CARTESIAN_POINT('Ctrl Pts',(-23.1157744392876,19.484919640127,23.512890187196));
#73317=CARTESIAN_POINT('Ctrl Pts',(-19.8951659330862,21.7183014710393,23.7117770985709));
#73318=CARTESIAN_POINT('Ctrl Pts',(-20.0332721107583,25.6350910028305,23.9106640099458));
#73319=CARTESIAN_POINT('Ctrl Pts',(-23.4031851045212,27.6360907448509,24.1095509213207));
#73320=CARTESIAN_POINT('Ctrl Pts',(-26.9082405945637,25.8825515908363,24.3084378326956));
#73321=CARTESIAN_POINT('Ctrl Pts',(-27.3275897653241,21.9858273480029,24.5073247440704));
#73322=CARTESIAN_POINT('Ctrl Pts',(-24.2758862836511,19.526677207255,24.7062116554454));
#73323=CARTESIAN_POINT('Ctrl Pts',(-20.5573869077351,20.7648516473877,24.9050985668202));
#73324=CARTESIAN_POINT('Ctrl Pts',(-19.589077286684,24.5625733359184,25.1039854781951));
#73325=CARTESIAN_POINT('Ctrl Pts',(-22.2607518642661,27.4300580383393,25.30287238957));
#73326=CARTESIAN_POINT('Ctrl Pts',(-26.1173682221808,26.7323304290285,25.5017593009449));
#73327=CARTESIAN_POINT('Ctrl Pts',(-27.6150229187122,23.1105430360612,25.7006462123198));
#73328=CARTESIAN_POINT('Ctrl Pts',(-25.3774982602538,19.8928113727298,25.8995331236947));
#73329=CARTESIAN_POINT('Ctrl Pts',(-21.4608897116096,20.0359580641337,26.0984200350696));
#73330=CARTESIAN_POINT('Ctrl Pts',(-19.4642284279858,23.4084433524528,26.2973069464445));
#73331=CARTESIAN_POINT('Ctrl Pts',(-21.2222768917239,26.9112393583044,26.4961938578193));
#73332=CARTESIAN_POINT('Ctrl Pts',(-25.11953752505,27.3255732364669,26.6950807691943));
#73333=CARTESIAN_POINT('Ctrl Pts',(-27.5747584232999,24.2707078565843,26.8939676805691));
#73334=CARTESIAN_POINT('Ctrl Pts',(-26.3317994016687,20.5538044091525,27.0928545919441));
#73335=CARTESIAN_POINT('Ctrl Pts',(-22.5328350720498,19.5903840672493,27.2917415033189));
#73336=CARTESIAN_POINT('Ctrl Pts',(-19.6687903145848,22.2657445766198,27.4906284146939));
#73337=CARTESIAN_POINT('Ctrl Pts',(-20.3714817712763,26.1214637581263,27.6895153260686));
#73338=CARTESIAN_POINT('Ctrl Pts',(-23.9951911518478,27.6144488190689,27.8884022374437));
#73339=CARTESIAN_POINT('Ctrl Pts',(-27.210045121279,25.3727990845368,28.0872891488183));
#73340=CARTESIAN_POINT('Ctrl Pts',(-27.0618496976934,21.4563514843679,28.2861760601934));
#73341=CARTESIAN_POINT('Ctrl Pts',(-23.6868136659813,19.4640820434689,28.4850629715682));
#73342=CARTESIAN_POINT('Ctrl Pts',(-20.1862527989148,21.2265423485704,28.6839498829432));
#73343=CARTESIAN_POINT('Ctrl Pts',(-19.7769918228223,25.1245114618019,28.882836794318));
#73344=CARTESIAN_POINT('Ctrl Pts',(-22.8349065564218,27.575461910994,29.081723705693));
#73345=CARTESIAN_POINT('Ctrl Pts',(-26.5504108930691,26.3283570624122,29.2806106170678));
#73346=CARTESIAN_POINT('Ctrl Pts',(-27.5085569433746,22.5269533007581,29.4794975284427));
#73347=CARTESIAN_POINT('Ctrl Pts',(-24.8302402232626,19.6686320185208,29.6783844398176));
#73348=CARTESIAN_POINT('Ctrl Pts',(-20.9740442903307,20.3719251481882,29.8772713511925));
#73349=CARTESIAN_POINT('Ctrl Pts',(-19.4884277064218,24.0062575140647,30.0761582625674));
#73350=CARTESIAN_POINT('Ctrl Pts',(-20.9816170272305,26.134253754113,30.2087495368173));
#73351=CARTESIAN_POINT('Ctrl Pts',(-22.0133720496472,26.646401067984,30.2750451739423));
#73352=CARTESIAN_POINT('Ctrl Pts',(-21.683763360871,20.9301056300456,-74.9968005183715));
#73353=CARTESIAN_POINT('Ctrl Pts',(-20.8100052970332,21.5524671541682,-74.930460688427));
#73354=CARTESIAN_POINT('Ctrl Pts',(-19.7500603056188,23.7286260299716,-74.7978252213578));
#73355=CARTESIAN_POINT('Ctrl Pts',(-21.6508572958594,26.850335879325,-74.5988941171632));
#73356=CARTESIAN_POINT('Ctrl Pts',(-25.2980779597533,26.9287941898422,-74.4000072057885));
#73357=CARTESIAN_POINT('Ctrl Pts',(-27.3384276727157,23.907745369296,-74.2011202944134));
#73358=CARTESIAN_POINT('Ctrl Pts',(-25.8981713831518,20.5555270839545,-74.0022333830388));
#73359=CARTESIAN_POINT('Ctrl Pts',(-22.3001619330665,19.9566147153388,-73.8033464716637));
#73360=CARTESIAN_POINT('Ctrl Pts',(-19.8509935044737,22.6592060284501,-73.6044595602889));
#73361=CARTESIAN_POINT('Ctrl Pts',(-20.8010702345145,26.1809879142899,-73.405572648914));
#73362=CARTESIAN_POINT('Ctrl Pts',(-24.2774443076499,27.2851381721642,-73.2066857375391));
#73363=CARTESIAN_POINT('Ctrl Pts',(-27.0855738978027,24.9573558052932,-73.0077988261642));
#73364=CARTESIAN_POINT('Ctrl Pts',(-26.6450518468136,21.3365062518087,-72.8089119147893));
#73365=CARTESIAN_POINT('Ctrl Pts',(-23.3606668817848,19.7499328594504,-72.6100250034144));
#73366=CARTESIAN_POINT('Ctrl Pts',(-20.2504975646859,21.6555146011386,-72.4111380920396));
#73367=CARTESIAN_POINT('Ctrl Pts',(-20.1725219599432,25.3022085555253,-72.2122511806645));
#73368=CARTESIAN_POINT('Ctrl Pts',(-23.198395070285,27.3389988568772,-72.0133642692899));
#73369=CARTESIAN_POINT('Ctrl Pts',(-26.5475949822429,25.8942549587852,-71.8144773579148));
#73370=CARTESIAN_POINT('Ctrl Pts',(-27.1424915123279,22.2955702762324,-71.61559044654));
#73371=CARTESIAN_POINT('Ctrl Pts',(-24.4364248862794,19.8498328915007,-71.416703535165));
#73372=CARTESIAN_POINT('Ctrl Pts',(-20.9160410567732,20.8044670497123,-71.2178166237902));
#73373=CARTESIAN_POINT('Ctrl Pts',(-19.8162741990877,24.2822454536544,-71.0189297124153));
#73374=CARTESIAN_POINT('Ctrl Pts',(-22.1477168554462,27.0873843233927,-70.8200428010404));
#73375=CARTESIAN_POINT('Ctrl Pts',(-25.7679708746349,26.6421990297343,-70.6211558896656));
#73376=CARTESIAN_POINT('Ctrl Pts',(-27.3503297725253,23.3557770296875,-70.4222689782906));
#73377=CARTESIAN_POINT('Ctrl Pts',(-25.4407398772024,20.2480615422864,-70.2233820669158));
#73378=CARTESIAN_POINT('Ctrl Pts',(-21.7939523994737,20.1747795865263,-70.0244951555408));
#73379=CARTESIAN_POINT('Ctrl Pts',(-19.7610558329135,23.2032710787019,-69.825608244166));
#73380=CARTESIAN_POINT('Ctrl Pts',(-21.2101097619757,26.5506091047579,-69.6267213327911));
#73381=CARTESIAN_POINT('Ctrl Pts',(-24.8095564848403,27.1408738296434,-69.4278344214162));
#73382=CARTESIAN_POINT('Ctrl Pts',(-27.2518096462275,24.4316620155666,-69.2289475100412));
#73383=CARTESIAN_POINT('Ctrl Pts',(-26.2926456595963,20.9125096173449,-69.0300605986664));
#73384=CARTESIAN_POINT('Ctrl Pts',(-22.8134549050434,19.8172193135151,-68.8311736872914));
#73385=CARTESIAN_POINT('Ctrl Pts',(-20.0113186992313,22.1522700282633,-68.6322867759167));
#73386=CARTESIAN_POINT('Ctrl Pts',(-20.4611626333522,25.7719481342452,-68.4333998645416));
#73387=CARTESIAN_POINT('Ctrl Pts',(-23.7496182724133,27.3500763502324,-68.2345129531669));
#73388=CARTESIAN_POINT('Ctrl Pts',(-26.854873699183,25.4364886489002,-68.0356260417919));
#73389=CARTESIAN_POINT('Ctrl Pts',(-26.9234624586994,21.7896098823126,-67.836739130417));
#73390=CARTESIAN_POINT('Ctrl Pts',(-23.8923572963366,19.7606124326231,-67.6378522190422));
#73391=CARTESIAN_POINT('Ctrl Pts',(-20.5468868609678,21.2139729254881,-67.4389653076672));
#73392=CARTESIAN_POINT('Ctrl Pts',(-19.9612548335806,24.8141762926101,-67.2400783962924));
#73393=CARTESIAN_POINT('Ctrl Pts',(-22.6736073939358,27.2529408865141,-67.0411914849174));
#73394=CARTESIAN_POINT('Ctrl Pts',(-26.1915225086404,26.2892488185399,-66.8423045735427));
#73395=CARTESIAN_POINT('Ctrl Pts',(-27.2823344572956,22.8086513915437,-66.6434176621676));
#73396=CARTESIAN_POINT('Ctrl Pts',(-24.9436795446887,20.0095225349377,-66.4445307507929));
#73397=CARTESIAN_POINT('Ctrl Pts',(-21.3245833502678,20.4640243409536,-66.2456438394179));
#73398=CARTESIAN_POINT('Ctrl Pts',(-19.7506884279502,23.7545081852605,-66.046756928043));
#73399=CARTESIAN_POINT('Ctrl Pts',(-21.6682707670623,26.8572984019637,-65.8478700166682));
#73400=CARTESIAN_POINT('Ctrl Pts',(-25.3152347821312,26.9211938551401,-65.6489831052932));
#73401=CARTESIAN_POINT('Ctrl Pts',(-27.3403297548654,23.8874800407619,-65.4500961939183));
#73402=CARTESIAN_POINT('Ctrl Pts',(-25.8826651050613,20.5438827377281,-65.2512092825435));
#73403=CARTESIAN_POINT('Ctrl Pts',(-22.2817110563076,19.9628843772254,-65.0523223711686));
#73404=CARTESIAN_POINT('Ctrl Pts',(-19.8464390688536,22.6783731920182,-64.8534354597936));
#73405=CARTESIAN_POINT('Ctrl Pts',(-20.8146576221548,26.1950451967957,-64.6545485484188));
#73406=CARTESIAN_POINT('Ctrl Pts',(-24.296655957123,27.2813769837839,-64.4556616370439));
#73407=CARTESIAN_POINT('Ctrl Pts',(-27.0927728286966,24.9391217464868,-64.2567747256691));
#73408=CARTESIAN_POINT('Ctrl Pts',(-26.6336139035149,21.3206134574858,-64.0578878142941));
#73409=CARTESIAN_POINT('Ctrl Pts',(-23.3411073035631,19.7509544354633,-63.8590009029193));
#73410=CARTESIAN_POINT('Ctrl Pts',(-20.2407874356726,21.6725282365198,-63.6601139915444));
#73411=CARTESIAN_POINT('Ctrl Pts',(-20.1815853946583,25.3195714600754,-63.4612270801694));
#73412=CARTESIAN_POINT('Ctrl Pts',(-23.2179028367071,27.3407606019554,-63.2623401687946));
#73413=CARTESIAN_POINT('Ctrl Pts',(-26.5596214698418,25.8787942093512,-63.0634532574197));
#73414=CARTESIAN_POINT('Ctrl Pts',(-27.135985201228,22.2770954427571,-62.8645663460447));
#73415=CARTESIAN_POINT('Ctrl Pts',(-24.4173646293078,19.8453200949762,-62.66567943467));
#73416=CARTESIAN_POINT('Ctrl Pts',(-20.9019415586626,20.8180635300704,-62.466792523295));
#73417=CARTESIAN_POINT('Ctrl Pts',(-19.8200917324914,24.3014570062308,-62.2679056119201));
#73418=CARTESIAN_POINT('Ctrl Pts',(-22.1659434153064,27.0945572619281,-62.0690187005452));
#73419=CARTESIAN_POINT('Ctrl Pts',(-25.783857806024,26.6307419780256,-61.8701317891703));
#73420=CARTESIAN_POINT('Ctrl Pts',(-27.3492783281297,23.3362180753784,-61.6712448777954));
#73421=CARTESIAN_POINT('Ctrl Pts',(-25.4237162475812,20.2383736909562,-61.4723579664206));
#73422=CARTESIAN_POINT('Ctrl Pts',(-21.7765998556609,20.1838651601527,-61.2734710550456));
#73423=CARTESIAN_POINT('Ctrl Pts',(-19.7593198920674,23.2227812012153,-61.0745841436708));
#73424=CARTESIAN_POINT('Ctrl Pts',(-21.2255856062074,26.5626156299977,-60.875697232296));
#73425=CARTESIAN_POINT('Ctrl Pts',(-24.8280231256177,27.1343437777115,-60.6768103209209));
#73426=CARTESIAN_POINT('Ctrl Pts',(-27.256297806293,24.4125959511606,-60.4779234095462));
#73427=CARTESIAN_POINT('Ctrl Pts',(-26.2790311004337,20.8984276367849,-60.2790364981711));
#73428=CARTESIAN_POINT('Ctrl Pts',(-22.794248252172,19.8210615631573,-60.0801495867964));
#73429=CARTESIAN_POINT('Ctrl Pts',(-20.0041692381986,22.1705058063621,-59.8812626754214));
#73430=CARTESIAN_POINT('Ctrl Pts',(-20.4726401126653,25.7878203069162,-59.6823757640466));
#73431=CARTESIAN_POINT('Ctrl Pts',(-23.7691758617172,27.3489997365033,-59.4834888526717));
#73432=CARTESIAN_POINT('Ctrl Pts',(-26.8645396321155,25.41945256552,-59.2846019412967));
#73433=CARTESIAN_POINT('Ctrl Pts',(-26.9143545624326,21.7722690454788,-59.0857150299219));
#73434=CARTESIAN_POINT('Ctrl Pts',(-23.8728449553169,19.7589016011293,-58.8868281185469));
#73435=CARTESIAN_POINT('Ctrl Pts',(-20.534900262219,21.2294642084204,-58.6879412071721));
#73436=CARTESIAN_POINT('Ctrl Pts',(-19.9678086450566,24.8326345143992,-58.4890542957972));
#73437=CARTESIAN_POINT('Ctrl Pts',(-22.6926792185619,27.2574045063341,-58.2901673844224));
#73438=CARTESIAN_POINT('Ctrl Pts',(-26.2055869566093,26.2756161482294,-58.0912804730474));
#73439=CARTESIAN_POINT('Ctrl Pts',(-27.2784674933923,22.7894496992577,-57.8923935616725));
#73440=CARTESIAN_POINT('Ctrl Pts',(-24.9254345808759,20.0023965478525,-57.6935066502976));
#73441=CARTESIAN_POINT('Ctrl Pts',(-21.3087259613717,20.4755222370161,-57.4946197389228));
#73442=CARTESIAN_POINT('Ctrl Pts',(-19.7517902098813,23.7740643728503,-57.2957328275478));
#73443=CARTESIAN_POINT('Ctrl Pts',(-21.6853192756418,26.866942402777,-57.0968459161729));
#73444=CARTESIAN_POINT('Ctrl Pts',(-25.3325638834496,26.9120636501059,-56.8979590047981));
#73445=CARTESIAN_POINT('Ctrl Pts',(-27.3420154740766,23.8679655141929,-56.6990720934231));
#73446=CARTESIAN_POINT('Ctrl Pts',(-25.8671584091358,20.5319160849822,-56.5001851820483));
#73447=CARTESIAN_POINT('Ctrl Pts',(-22.2632612840498,19.9694619375712,-56.3012982706734));
#73448=CARTESIAN_POINT('Ctrl Pts',(-19.8419999966857,22.6974507451831,-56.1024113592985));
#73449=CARTESIAN_POINT('Ctrl Pts',(-20.8283083810279,26.2090920889309,-55.9035244479236));
#73450=CARTESIAN_POINT('Ctrl Pts',(-24.3158526570263,27.2774853119971,-55.7046375365487));
#73451=CARTESIAN_POINT('Ctrl Pts',(-27.0998753300306,24.9208676271909,-55.5057506251739));
#73452=CARTESIAN_POINT('Ctrl Pts',(-26.6220956097466,21.3047708786195,-55.3068637137989));
#73453=CARTESIAN_POINT('Ctrl Pts',(-23.3215525500752,19.7520813837756,-55.1079768024241));
#73454=CARTESIAN_POINT('Ctrl Pts',(-20.231165382951,21.6895891420612,-54.9090898910491));
#73455=CARTESIAN_POINT('Ctrl Pts',(-20.1907378933386,25.3368887971795,-54.7102029796743));
#73456=CARTESIAN_POINT('Ctrl Pts',(-23.2374195165061,27.3424212060917,-54.5113160682993));
#73457=CARTESIAN_POINT('Ctrl Pts',(-26.5715681567657,25.8632721261143,-54.3124291569246));
#73458=CARTESIAN_POINT('Ctrl Pts',(-27.129383902906,22.2586541505862,-54.1135422455495));
#73459=CARTESIAN_POINT('Ctrl Pts',(-24.3982813791998,19.8409055778124,-53.9146553341748));
#73460=CARTESIAN_POINT('Ctrl Pts',(-20.8879122456252,20.8317323548981,-53.7157684227997));
#73461=CARTESIAN_POINT('Ctrl Pts',(-19.8240081057162,24.3206486819583,-53.516881511425));
#73462=CARTESIAN_POINT('Ctrl Pts',(-22.1842066598536,27.1016362657478,-53.31799460005));
#73463=CARTESIAN_POINT('Ctrl Pts',(-25.7996855486223,26.6192033056276,-53.1191076886752));
#73464=CARTESIAN_POINT('Ctrl Pts',(-27.3481262153026,23.3166647883784,-52.9202207773002));
#73465=CARTESIAN_POINT('Ctrl Pts',(-25.4066429733337,20.2287736022619,-52.7213338659254));
#73466=CARTESIAN_POINT('Ctrl Pts',(-21.7592943114516,20.1930399373209,-52.5224469545505));
#73467=CARTESIAN_POINT('Ctrl Pts',(-19.7576844057563,23.2423000019213,-52.3235600431756));
#73468=CARTESIAN_POINT('Ctrl Pts',(-21.2411230510481,26.574542331314,-52.1246731318007));
#73469=CARTESIAN_POINT('Ctrl Pts',(-24.8464559071597,27.1277187523461,-51.9257862204258));
#73470=CARTESIAN_POINT('Ctrl Pts',(-27.2606877611413,24.3935070357146,-51.7268993090509));
#73471=CARTESIAN_POINT('Ctrl Pts',(-26.2653442322895,20.8844159260802,-51.528012397676));
#73472=CARTESIAN_POINT('Ctrl Pts',(-22.7750616324048,19.8250026313341,-51.3291254863012));
#73473=CARTESIAN_POINT('Ctrl Pts',(-19.9971137436173,22.1887781459135,-51.1302385749262));
#73474=CARTESIAN_POINT('Ctrl Pts',(-20.4841991445828,25.8036331870332,-50.9313516635514));
#73475=CARTESIAN_POINT('Ctrl Pts',(-23.7887276498457,27.3478224610695,-50.7324647521764));
#73476=CARTESIAN_POINT('Ctrl Pts',(-26.874117740883,25.4023669508426,-50.5335778408016));
#73477=CARTESIAN_POINT('Ctrl Pts',(-26.9051575219715,21.7549753228249,-50.3346909294266));
#73478=CARTESIAN_POINT('Ctrl Pts',(-23.8533240660305,19.7572912353521,-50.1358040180519));
#73479=CARTESIAN_POINT('Ctrl Pts',(-20.522993566263,21.2450169891325,-49.9369171066769));
#73480=CARTESIAN_POINT('Ctrl Pts',(-19.9744573864931,24.8510587547845,-49.738030195302));
#73481=CARTESIAN_POINT('Ctrl Pts',(-22.7117737677313,27.2617698915965,-49.5391432839272));
#73482=CARTESIAN_POINT('Ctrl Pts',(-26.2195810417756,26.2619112594362,-49.3402563725522));
#73483=CARTESIAN_POINT('Ctrl Pts',(-27.2745017367903,22.770268167227,-49.1413694611774));
#73484=CARTESIAN_POINT('Ctrl Pts',(-24.9071531765824,19.9953645741946,-48.9424825498024));
#73485=CARTESIAN_POINT('Ctrl Pts',(-21.2929279699248,20.4871016093095,-48.7435956384276));
#73486=CARTESIAN_POINT('Ctrl Pts',(-19.752992645972,23.7936146297263,-48.5447087270527));
#73487=CARTESIAN_POINT('Ctrl Pts',(-21.7024172024526,26.8764985157549,-48.3458218156778));
#73488=CARTESIAN_POINT('Ctrl Pts',(-25.3498457559064,26.9028443615838,-48.1469349043029));
#73489=CARTESIAN_POINT('Ctrl Pts',(-27.343600716653,23.8484425686559,-47.948047992928));
#73490=CARTESIAN_POINT('Ctrl Pts',(-25.8515903183102,20.520029414106,-47.7491610815531));
#73491=CARTESIAN_POINT('Ctrl Pts',(-22.2448456153347,19.9761343840675,-47.5502741701782));
#73492=CARTESIAN_POINT('Ctrl Pts',(-19.8376591882389,22.716550896452,-47.3513872588034));
#73493=CARTESIAN_POINT('Ctrl Pts',(-20.8420312677722,26.2230685253821,-47.1525003474284));
#73494=CARTESIAN_POINT('Ctrl Pts',(-24.3350290695526,27.2734948735382,-46.9536134360536));
#73495=CARTESIAN_POINT('Ctrl Pts',(-27.1068837711188,24.9025771884323,-46.7547265246786));
#73496=CARTESIAN_POINT('Ctrl Pts',(-26.6104959162545,21.2889878020069,-46.5558396133039));
#73497=CARTESIAN_POINT('Ctrl Pts',(-23.3020038568303,19.7533089785318,-46.3569527019288));
#73498=CARTESIAN_POINT('Ctrl Pts',(-20.2216312815894,21.706699352688,-46.1580657905541));
#73499=CARTESIAN_POINT('Ctrl Pts',(-20.1999794146531,25.3541587908178,-45.959178879179));
#73500=CARTESIAN_POINT('Ctrl Pts',(-23.2569444859605,27.3439813228416,-45.7602919678043));
#73501=CARTESIAN_POINT('Ctrl Pts',(-26.5834347828758,25.8476887509589,-45.5614050564293));
#73502=CARTESIAN_POINT('Ctrl Pts',(-27.1226877624005,22.240247084041,-45.3625181450545));
#73503=CARTESIAN_POINT('Ctrl Pts',(-24.3791756574643,19.8365893533705,-45.1636312336795));
#73504=CARTESIAN_POINT('Ctrl Pts',(-20.8739534810364,20.8454732168662,-44.9647443223047));
#73505=CARTESIAN_POINT('Ctrl Pts',(-19.8280232194233,24.3398199432207,-44.7658574109297));
#73506=CARTESIAN_POINT('Ctrl Pts',(-22.2025061027852,27.1086211626593,-44.5669704995549));
#73507=CARTESIAN_POINT('Ctrl Pts',(-25.8154536842612,26.6075833101481,-44.3680835881799));
#73508=CARTESIAN_POINT('Ctrl Pts',(-27.3468734639142,23.2971176911406,-44.1691966768052));
#73509=CARTESIAN_POINT('Ctrl Pts',(-25.3895205072279,20.2192615283065,-43.9703097654301));
#73510=CARTESIAN_POINT('Ctrl Pts',(-21.7420362252341,20.2023036761223,-43.7714228540554));
#73511=CARTESIAN_POINT('Ctrl Pts',(-19.7561494174165,23.2618269629562,-43.5725359426803));
#73512=CARTESIAN_POINT('Ctrl Pts',(-21.2567216847247,26.5863888930049,-43.3736490313055));
#73513=CARTESIAN_POINT('Ctrl Pts',(-24.86485434105,27.1209989289215,-43.1747621199306));
#73514=CARTESIAN_POINT('Ctrl Pts',(-27.2649793944301,24.3743957751549,-42.9758752085558));
#73515=CARTESIAN_POINT('Ctrl Pts',(-26.2515854178548,20.8704748564718,-42.7769882971808));
#73516=CARTESIAN_POINT('Ctrl Pts',(-22.7558955541571,19.8290424136397,-42.578101385806));
#73517=CARTESIAN_POINT('Ctrl Pts',(-19.9901524024507,22.207086562711,-42.379214474431));
#73518=CARTESIAN_POINT('Ctrl Pts',(-20.4958394228052,25.8193863555838,-42.1803275630562));
#73519=CARTESIAN_POINT('Ctrl Pts',(-23.8082731187033,27.3465445551235,-41.9814406516812));
#73520=CARTESIAN_POINT('Ctrl Pts',(-26.8836077716783,25.3852322576158,-41.7825537403064));
#73521=CARTESIAN_POINT('Ctrl Pts',(-26.8958715810256,21.7377291726105,-41.5836668289315));
#73522=CARTESIAN_POINT('Ctrl Pts',(-23.8337951457545,19.7557813779647,-41.3847799175566));
#73523=CARTESIAN_POINT('Ctrl Pts',(-20.5111670886113,21.2606308554963,-41.1858930061817));
#73524=CARTESIAN_POINT('Ctrl Pts',(-19.9812008817077,24.8694485255489,-40.9870060948069));
#73525=CARTESIAN_POINT('Ctrl Pts',(-22.7308905354638,27.2660369266243,-40.7881191834319));
#73526=CARTESIAN_POINT('Ctrl Pts',(-26.2335043933146,26.248134515322,-40.5892322720571));
#73527=CARTESIAN_POINT('Ctrl Pts',(-27.270437292577,22.7511073037364,-40.3903453606822));
#73528=CARTESIAN_POINT('Ctrl Pts',(-24.8888358162407,19.9884268003022,-40.1914584493072));
#73529=CARTESIAN_POINT('Ctrl Pts',(-21.2771897945526,20.4987621509962,-39.9925715379324));
#73530=CARTESIAN_POINT('Ctrl Pts',(-19.7542957043592,23.8131584378329,-39.7936846265574));
#73531=CARTESIAN_POINT('Ctrl Pts',(-21.7195640944224,26.8859664876731,-39.5947977151827));
#73532=CARTESIAN_POINT('Ctrl Pts',(-25.3670799415552,26.8935362338724,-39.3959108038077));
#73533=CARTESIAN_POINT('Ctrl Pts',(-27.3450854405875,23.8289117214825,-39.1970238924328));
#73534=CARTESIAN_POINT('Ctrl Pts',(-25.8359612451185,20.5082230400801,-38.9981369810579));
#73535=CARTESIAN_POINT('Ctrl Pts',(-22.2264645381529,19.9829015399035,-38.799250069683));
#73536=CARTESIAN_POINT('Ctrl Pts',(-19.833416758539,22.7356731396968,-38.6003631583082));
#73537=CARTESIAN_POINT('Ctrl Pts',(-20.8558259187495,26.2369741357925,-38.4014762469333));
#73538=CARTESIAN_POINT('Ctrl Pts',(-24.3541846865526,27.2694057741485,-38.2025893355583));
#73539=CARTESIAN_POINT('Ctrl Pts',(-27.1137979662469,24.8842509148831,-38.0037024241835));
#73540=CARTESIAN_POINT('Ctrl Pts',(-26.5988151304152,21.2732646458782,-37.8048155128086));
#73541=CARTESIAN_POINT('Ctrl Pts',(-23.2824617418424,19.7546371872021,-37.6059286014337));
#73542=CARTESIAN_POINT('Ctrl Pts',(-20.2121853842287,21.7238584150028,-37.4070416900588));
#73543=CARTESIAN_POINT('Ctrl Pts',(-20.209309713714,25.3713809833582,-37.2081547786839));
#73544=CARTESIAN_POINT('Ctrl Pts',(-23.276477227685,27.3454409108643,-37.009267867309));
#73545=CARTESIAN_POINT('Ctrl Pts',(-26.5952210337223,25.8320444968236,-36.8103809559342));
#73546=CARTESIAN_POINT('Ctrl Pts',(-27.1158969571505,22.2218747308839,-36.6114940445593));
#73547=CARTESIAN_POINT('Ctrl Pts',(-24.360047970377,19.8323715360244,-36.4126071331843));
#73548=CARTESIAN_POINT('Ctrl Pts',(-20.8600656347848,20.8592857518602,-36.2137202218095));
#73549=CARTESIAN_POINT('Ctrl Pts',(-19.8321369672173,24.358970282005,-36.0148333104345));
#73550=CARTESIAN_POINT('Ctrl Pts',(-22.2208412591905,27.1155117675722,-35.8159463990597));
#73551=CARTESIAN_POINT('Ctrl Pts',(-25.8311617951063,26.5958822995014,-35.6170594876848));
#73552=CARTESIAN_POINT('Ctrl Pts',(-27.3455201071605,23.2775773016365,-35.4181725763099));
#73553=CARTESIAN_POINT('Ctrl Pts',(-25.3723493029866,20.2098377211476,-35.219285664935));
#73554=CARTESIAN_POINT('Ctrl Pts',(-21.7248260543247,20.2116561310803,-35.0203987535601));
#73555=CARTESIAN_POINT('Ctrl Pts',(-19.7547149677231,23.2813615668823,-34.8215118421852));
#73556=CARTESIAN_POINT('Ctrl Pts',(-21.2723810938942,26.5981550011522,-34.6226249308104));
#73557=CARTESIAN_POINT('Ctrl Pts',(-24.8832179397545,27.1141844855041,-34.4237380194354));
#73558=CARTESIAN_POINT('Ctrl Pts',(-27.2691725924367,24.3552626759039,-34.2248511080606));
#73559=CARTESIAN_POINT('Ctrl Pts',(-26.23775502172,20.8566047973795,-34.0259641966856));
#73560=CARTESIAN_POINT('Ctrl Pts',(-22.7367505253045,19.8331808030248,-33.8270772853108));
#73561=CARTESIAN_POINT('Ctrl Pts',(-19.9832853991652,22.2254305716062,-33.6281903739359));
#73562=CARTESIAN_POINT('Ctrl Pts',(-20.5075606388801,25.8350793951297,-33.429303462561));
#73563=CARTESIAN_POINT('Ctrl Pts',(-23.8278117503613,27.3451660525278,-33.2304165511861));
#73564=CARTESIAN_POINT('Ctrl Pts',(-26.8930094730282,25.3680489398862,-33.0315296398112));
#73565=CARTESIAN_POINT('Ctrl Pts',(-26.8864969856598,21.7205310518353,-32.8326427284363));
#73566=CARTESIAN_POINT('Ctrl Pts',(-23.8142587119796,19.7543720689762,-32.6337558170614));
#73567=CARTESIAN_POINT('Ctrl Pts',(-20.4994211426499,21.2763053937652,-32.4348689056866));
#73568=CARTESIAN_POINT('Ctrl Pts',(-19.9880389520064,24.8878033393877,-32.2359819943116));
#73569=CARTESIAN_POINT('Ctrl Pts',(-22.750029015191,27.2702054983469,-32.0370950829368));
#73570=CARTESIAN_POINT('Ctrl Pts',(-26.2473566422763,26.2342862809518,-31.8382081715618));
#73571=CARTESIAN_POINT('Ctrl Pts',(-27.2662742684546,22.7319676165231,-31.639321260187));
#73572=CARTESIAN_POINT('Ctrl Pts',(-24.8704829852364,19.9815834100169,-31.4404343488121));
#73573=CARTESIAN_POINT('Ctrl Pts',(-21.2615118522959,20.5105035530874,-31.2415474374372));
#73574=CARTESIAN_POINT('Ctrl Pts',(-19.7556993505138,23.8326952792856,-31.0426605260623));
#73575=CARTESIAN_POINT('Ctrl Pts',(-21.7367594971816,26.8953460676431,-30.8437736146875));
#73576=CARTESIAN_POINT('Ctrl Pts',(-25.3842659837132,26.8841395136247,-30.6448867033125));
#73577=CARTESIAN_POINT('Ctrl Pts',(-27.3464696065371,23.8093734902142,-30.4459997919377));
#73578=CARTESIAN_POINT('Ctrl Pts',(-25.8202716037099,20.496497275758,-30.2471128805627));
#73579=CARTESIAN_POINT('Ctrl Pts',(-22.2081185395785,19.9897632257587,-30.0482259691879));
#73580=CARTESIAN_POINT('Ctrl Pts',(-19.8292728200044,22.7548169682034,-29.849339057813));
#73581=CARTESIAN_POINT('Ctrl Pts',(-20.86969196842,26.250808551682,-29.6504521464381));
#73582=CARTESIAN_POINT('Ctrl Pts',(-24.3733190004281,27.2652181221834,-29.4515652350632));
#73583=CARTESIAN_POINT('Ctrl Pts',(-27.1206177321983,24.865889292165,-29.2526783236883));
#73584=CARTESIAN_POINT('Ctrl Pts',(-26.5870535617536,21.2576018268762,-29.0537914123134));
#73585=CARTESIAN_POINT('Ctrl Pts',(-23.2629267229515,19.7560659745909,-28.8549045009385));
#73586=CARTESIAN_POINT('Ctrl Pts',(-20.2028279411726,21.7410658743133,-28.6560175895637));
#73587=CARTESIAN_POINT('Ctrl Pts',(-20.2187285432812,25.3885549184361,-28.4571306781887));
#73588=CARTESIAN_POINT('Ctrl Pts',(-23.2960172240878,27.3467999314825,-28.2582437668139));
#73589=CARTESIAN_POINT('Ctrl Pts',(-26.6069265969855,25.81633977826,-28.0593568554389));
#73590=CARTESIAN_POINT('Ctrl Pts',(-27.109011667103,22.2035375779578,-27.8604699440641));
#73591=CARTESIAN_POINT('Ctrl Pts',(-24.3408988247963,19.8282522375408,-27.6615830326892));
#73592=CARTESIAN_POINT('Ctrl Pts',(-20.8462490748795,20.8731695938664,-27.4626961213143));
#73593=CARTESIAN_POINT('Ctrl Pts',(-19.8363492400895,24.3780991908532,-27.2638092099394));
#73594=CARTESIAN_POINT('Ctrl Pts',(-22.2392116432122,27.1223078978946,-27.0649222985645));
#73595=CARTESIAN_POINT('Ctrl Pts',(-25.8468094649135,26.5841005837488,-26.8660353871896));
#73596=CARTESIAN_POINT('Ctrl Pts',(-27.3440661809039,23.2580441376607,-26.6671484758148));
#73597=CARTESIAN_POINT('Ctrl Pts',(-25.3551298156233,20.2005024305031,-26.4682615644398));
#73598=CARTESIAN_POINT('Ctrl Pts',(-21.70766425477,20.2210970543674,-26.269374653065));
#73599=CARTESIAN_POINT('Ctrl Pts',(-19.753381094687,23.3009032960584,-26.0704877416901));
#73600=CARTESIAN_POINT('Ctrl Pts',(-21.2881008636032,26.6098403439699,-25.8716008303151));
#73601=CARTESIAN_POINT('Ctrl Pts',(-24.9015462166627,27.1072756026676,-25.6727139189403));
#73602=CARTESIAN_POINT('Ctrl Pts',(-27.2732672440469,24.3361082449633,-25.4738270075654));
#73603=CARTESIAN_POINT('Ctrl Pts',(-26.223853410372,20.8428061163415,-25.2749400961905));
#73604=CARTESIAN_POINT('Ctrl Pts',(-22.7176270531645,19.8374176898278,-25.0760531848156));
#73605=CARTESIAN_POINT('Ctrl Pts',(-19.976512915727,22.2438096865073,-24.8771662734407));
#73606=CARTESIAN_POINT('Ctrl Pts',(-20.5193624822115,25.8507118898268,-24.6782793620658));
#73607=CARTESIAN_POINT('Ctrl Pts',(-23.8473430270719,27.3436869898112,-24.4793924506909));
#73608=CARTESIAN_POINT('Ctrl Pts',(-26.9023225958004,25.3508174529887,-24.2805055393161));
#73609=CARTESIAN_POINT('Ctrl Pts',(-26.8770339842884,21.7033814162266,-24.0816186279412));
#73610=CARTESIAN_POINT('Ctrl Pts',(-23.7947152823949,19.7530633457313,-23.8827317165663));
#73611=CARTESIAN_POINT('Ctrl Pts',(-20.4877560396305,21.2920401885848,-23.6838448051914));
#73612=CARTESIAN_POINT('Ctrl Pts',(-19.9949714161898,24.9061227099231,-23.4849578938165));
#73613=CARTESIAN_POINT('Ctrl Pts',(-22.7691886997684,27.2742754963025,-23.2860709824416));
#73614=CARTESIAN_POINT('Ctrl Pts',(-26.2611374215946,26.2203669232854,-23.0871840710667));
#73615=CARTESIAN_POINT('Ctrl Pts',(-27.2620127747377,22.712849612763,-22.8882971596918));
#73616=CARTESIAN_POINT('Ctrl Pts',(-24.8520951698951,19.9748345846794,-22.6894102483169));
#73617=CARTESIAN_POINT('Ctrl Pts',(-21.2458945585992,20.5223255044515,-22.4905233369421));
#73618=CARTESIAN_POINT('Ctrl Pts',(-19.7572035472408,23.8522246363839,-22.2916364255671));
#73619=CARTESIAN_POINT('Ctrl Pts',(-21.7540029550752,26.9046370071187,-22.0927495141923));
#73620=CARTESIAN_POINT('Ctrl Pts',(-25.4014034269733,26.8746544498414,-21.8938626028174));
#73621=CARTESIAN_POINT('Ctrl Pts',(-27.3477531778232,23.7898283925879,-21.6949756914425));
#73622=CARTESIAN_POINT('Ctrl Pts',(-25.8045218098391,20.4848524318565,-21.4960887800676));
#73623=CARTESIAN_POINT('Ctrl Pts',(-22.1898081057556,19.9967192598074,-21.2972018686927));
#73624=CARTESIAN_POINT('Ctrl Pts',(-19.8252274824439,22.773981874686,-21.0983149573178));
#73625=CARTESIAN_POINT('Ctrl Pts',(-20.883629049352,26.2645714064571,-20.8994280459429));
#73626=CARTESIAN_POINT('Ctrl Pts',(-24.3924315041455,27.2609320286103,-20.700541134568));
#73627=CARTESIAN_POINT('Ctrl Pts',(-27.1273428882579,24.8474928068367,-20.5016542231931));
#73628=CARTESIAN_POINT('Ctrl Pts',(-26.575211521936,21.2419997600445,-20.3027673118182));
#73629=CARTESIAN_POINT('Ctrl Pts',(-23.2433993178095,19.7575953028371,-20.1038804004434));
#73630=CARTESIAN_POINT('Ctrl Pts',(-20.1935592003809,21.7583212746448,-19.9049934890685));
#73631=CARTESIAN_POINT('Ctrl Pts',(-20.2282356537676,25.405680140965,-19.7061065776936));
#73632=CARTESIAN_POINT('Ctrl Pts',(-23.3155639573856,27.348058348684,-19.5072196663187));
#73633=CARTESIAN_POINT('Ctrl Pts',(-26.6185511624836,25.8005750114223,-19.3083327549438));
#73634=CARTESIAN_POINT('Ctrl Pts',(-27.1020320747092,22.1852361111728,-19.1094458435689));
#73635=CARTESIAN_POINT('Ctrl Pts',(-24.3217287281487,19.8242315670756,-18.910558932194));
#73636=CARTESIAN_POINT('Ctrl Pts',(-20.8325041674413,20.8871243749818,-18.7116720208192));
#73637=CARTESIAN_POINT('Ctrl Pts',(-19.8406599264202,24.3972061628746,-18.5127851094442));
#73638=CARTESIAN_POINT('Ctrl Pts',(-22.25761676806,27.1290093735385,-18.3138981980694));
#73639=CARTESIAN_POINT('Ctrl Pts',(-25.8623962790404,26.5722384750899,-18.1150112866944));
#73640=CARTESIAN_POINT('Ctrl Pts',(-27.3425117236713,23.2385187168156,-17.9161243753196));
#73641=CARTESIAN_POINT('Ctrl Pts',(-25.3378625014317,20.1912559037459,-17.7172374639446));
#73642=CARTESIAN_POINT('Ctrl Pts',(-21.6905512813346,20.2306261958117,-17.5183505525698));
#73643=CARTESIAN_POINT('Ctrl Pts',(-19.7521478336541,23.320451632655,-17.3194636411949));
#73644=CARTESIAN_POINT('Ctrl Pts',(-21.3038805772987,26.6214446118121,-17.12057672982));
#73645=CARTESIAN_POINT('Ctrl Pts',(-24.9198386860995,27.1002724634881,-16.9216898184451));
#73646=CARTESIAN_POINT('Ctrl Pts',(-27.2772632407584,24.3169329898997,-16.7228029070702));
#73647=CARTESIAN_POINT('Ctrl Pts',(-26.2098809521846,20.8290791790038,-16.5239159956953));
#73648=CARTESIAN_POINT('Ctrl Pts',(-22.6985256444836,19.841752961777,-16.3250290843204));
#73649=CARTESIAN_POINT('Ctrl Pts',(-19.9698351315979,22.2622234203925,-16.1261421729455));
#73650=CARTESIAN_POINT('Ctrl Pts',(-20.531244640066,25.8662834254346,-15.9272552615707));
#73651=CARTESIAN_POINT('Ctrl Pts',(-23.8668664312827,27.3421074061667,-15.7283683501957));
#73652=CARTESIAN_POINT('Ctrl Pts',(-26.9115468932093,25.3335382535345,-15.5294814388209));
#73653=CARTESIAN_POINT('Ctrl Pts',(-26.8674828276681,21.6862807202267,-15.330594527446));
#73654=CARTESIAN_POINT('Ctrl Pts',(-23.7751653748748,19.7518552429097,-15.1317076160711));
#73655=CARTESIAN_POINT('Ctrl Pts',(-20.4761720886628,21.3078348230044,-14.9328207046962));
#73656=CARTESIAN_POINT('Ctrl Pts',(-20.0019980905566,24.9244061517165,-14.7339337933213));
#73657=CARTESIAN_POINT('Ctrl Pts',(-22.7883690814905,27.2782468126418,-14.5350468819464));
#73658=CARTESIAN_POINT('Ctrl Pts',(-26.2748463660975,26.2063768111669,-14.3361599705715));
#73659=CARTESIAN_POINT('Ctrl Pts',(-27.2576529243502,22.6937537990577,-14.1372730591966));
#73660=CARTESIAN_POINT('Ctrl Pts',(-24.8336728574687,19.9681805031243,-13.9383861478217));
#73661=CARTESIAN_POINT('Ctrl Pts',(-21.2303383272995,20.5342276918229,-13.7394992364469));
#73662=CARTESIAN_POINT('Ctrl Pts',(-19.7588082546812,23.8717459916262,-13.540612325072));
#73663=CARTESIAN_POINT('Ctrl Pts',(-21.7712940111747,26.9138390599026,-13.3417254136971));
#73664=CARTESIAN_POINT('Ctrl Pts',(-25.4184918172162,26.8650812938635,-13.1428385023222));
#73665=CARTESIAN_POINT('Ctrl Pts',(-27.3489361204329,23.7702769465225,-12.9439515909473));
#73666=CARTESIAN_POINT('Ctrl Pts',(-25.7887122808542,20.4732888169482,-12.7450646795724));
#73667=CARTESIAN_POINT('Ctrl Pts',(-22.1715337218863,20.0037694577242,-12.5461777681975));
#73668=CARTESIAN_POINT('Ctrl Pts',(-19.8212808530538,22.7931673513006,-12.3472908568226));
#73669=CARTESIAN_POINT('Ctrl Pts',(-20.8976367922315,26.2782623354208,-12.1484039454477));
#73670=CARTESIAN_POINT('Ctrl Pts',(-24.4115216912494,27.2565476070049,-11.9495170340728));
#73671=CARTESIAN_POINT('Ctrl Pts',(-27.1339732562184,24.8290619463798,-11.750630122698));
#73672=CARTESIAN_POINT('Ctrl Pts',(-26.56328932476,21.2264588588168,-11.551743211323));
#73673=CARTESIAN_POINT('Ctrl Pts',(-23.2238800438662,19.7592251314157,-11.3528562999482));
#73674=CARTESIAN_POINT('Ctrl Pts',(-20.1843794074626,21.7756241587528,-11.1539693885733));
#73675=CARTESIAN_POINT('Ctrl Pts',(-20.2378307932482,25.4227561971494,-10.9550824771984));
#73676=CARTESIAN_POINT('Ctrl Pts',(-23.335116909616,27.3492161291226,-10.7561955658235));
#73677=CARTESIAN_POINT('Ctrl Pts',(-26.630094422181,25.7847506140553,-10.5573086544486));
#73678=CARTESIAN_POINT('Ctrl Pts',(-27.0949583649188,22.1669708154931,-10.3584217430737));
#73679=CARTESIAN_POINT('Ctrl Pts',(-24.3025381884162,19.8203096311709,-10.1595348316988));
#73680=CARTESIAN_POINT('Ctrl Pts',(-20.8188312766913,20.9011497254233,-9.96064792032392));
#73681=CARTESIAN_POINT('Ctrl Pts',(-19.8450689119821,24.4162906917602,-9.76176100894904));
#73682=CARTESIAN_POINT('Ctrl Pts',(-22.2760561460228,27.1356160169234,-9.56287409757416));
#73683=CARTESIAN_POINT('Ctrl Pts',(-25.8779218244577,26.5602962878544,-9.36398718619925));
#73684=CARTESIAN_POINT('Ctrl Pts',(-27.3408567766537,23.2190015564985,-9.16510027482437));
#73685=CARTESIAN_POINT('Ctrl Pts',(-25.3205478179721,20.1820983858963,-8.96621336344948));
#73686=CARTESIAN_POINT('Ctrl Pts',(-21.6734875874893,20.2402433029038,-8.76732645207459));
#73687=CARTESIAN_POINT('Ctrl Pts',(-19.7510152173042,23.3400060586673,-8.56843954069969));
#73688=CARTESIAN_POINT('Ctrl Pts',(-21.3197198168398,26.6329674971811,-8.36955262932482));
#73689=CARTESIAN_POINT('Ctrl Pts',(-24.9380948633393,27.0931752535394,-8.17066571794991));
#73690=CARTESIAN_POINT('Ctrl Pts',(-27.2811604766821,24.2977374188318,-7.97177880657503));
#73691=CARTESIAN_POINT('Ctrl Pts',(-26.1958380174094,20.8154243491121,-7.77289189520014));
#73692=CARTESIAN_POINT('Ctrl Pts',(-22.6794468054235,19.8461865039934,-7.57400498382525));
#73693=CARTESIAN_POINT('Ctrl Pts',(-19.96325222373,22.2806712853224,-7.37511807245035));
#73694=CARTESIAN_POINT('Ctrl Pts',(-20.5432067975827,25.8817935893286,-7.17623116107547));
#73695=CARTESIAN_POINT('Ctrl Pts',(-23.8863814456496,27.340427343451,-6.97734424970057));
#73696=CARTESIAN_POINT('Ctrl Pts',(-26.9206821208237,25.3162117993992,-6.77845733832569));
#73697=CARTESIAN_POINT('Ctrl Pts',(-26.8578437688918,21.6692294169808,-6.57957042695078));
#73698=CARTESIAN_POINT('Ctrl Pts',(-23.755609507466,19.7507477925242,-6.38068351557592));
#73699=CARTESIAN_POINT('Ctrl Pts',(-20.4646695967059,21.3236888784871,-6.18179660420101));
#73700=CARTESIAN_POINT('Ctrl Pts',(-20.0091187889095,24.942653180281,-5.98290969282612));
#73701=CARTESIAN_POINT('Ctrl Pts',(-22.8075696521026,27.2821193421303,-5.78402278145123));
#73702=CARTESIAN_POINT('Ctrl Pts',(-26.2884831125161,26.1923163153157,-5.58513587007634));
#73703=CARTESIAN_POINT('Ctrl Pts',(-27.253194832822,22.6746806814207,-5.38624895870145));
#73704=CARTESIAN_POINT('Ctrl Pts',(-24.8152165361243,19.9616213416763,-5.18736204732655));
#73705=CARTESIAN_POINT('Ctrl Pts',(-21.2148435706164,20.5462097998092,-4.98847513595167));
#73706=CARTESIAN_POINT('Ctrl Pts',(-19.7605134303124,23.891258827723,-4.78958822457678));
#73707=CARTESIAN_POINT('Ctrl Pts',(-21.7886322072903,26.9229519821522,-4.59070131320189));
#73708=CARTESIAN_POINT('Ctrl Pts',(-25.4355307016224,26.8554202993672,-4.39181440182699));
#73709=CARTESIAN_POINT('Ctrl Pts',(-27.3500184030198,23.7507196701049,-4.19292749045211));
#73710=CARTESIAN_POINT('Ctrl Pts',(-25.7728434356868,20.4618067374535,-3.99404057907722));
#73711=CARTESIAN_POINT('Ctrl Pts',(-22.1532958722172,20.0109136326883,-3.79515366770233));
#73712=CARTESIAN_POINT('Ctrl Pts',(-19.8174330364143,22.8123728896575,-3.59626675632743));
#73713=CARTESIAN_POINT('Ctrl Pts',(-20.9117148258723,26.2918809757817,-3.39737984495255));
#73714=CARTESIAN_POINT('Ctrl Pts',(-24.4305890558748,27.2520649735484,-3.19849293357766));
#73715=CARTESIAN_POINT('Ctrl Pts',(-27.1405086603839,24.8105971991879,-2.99960602220276));
#73716=CARTESIAN_POINT('Ctrl Pts',(-26.5512872861481,21.2109795350063,-2.80071911082788));
#73717=CARTESIAN_POINT('Ctrl Pts',(-23.2043694183563,19.7609554171384,-2.60183219945298));
#73718=CARTESIAN_POINT('Ctrl Pts',(-20.17528880567,21.7929740681333,-2.40294528807809));
#73719=CARTESIAN_POINT('Ctrl Pts',(-20.2475137074644,25.4397826344972,-2.2040583767032));
#73720=CARTESIAN_POINT('Ctrl Pts',(-23.3546755626521,27.3502732421183,-2.00517146532831));
#73721=CARTESIAN_POINT('Ctrl Pts',(-26.641556070197,25.7688670054847,-1.80628455395342));
#73722=CARTESIAN_POINT('Ctrl Pts',(-27.0877907251756,22.1487421749243,-1.60739764257854));
#73723=CARTESIAN_POINT('Ctrl Pts',(-24.2833277141221,19.8164865337531,-1.40851073120364));
#73724=CARTESIAN_POINT('Ctrl Pts',(-20.805230764943,20.915245273538,-1.20962381982875));
#73725=CARTESIAN_POINT('Ctrl Pts',(-19.8495760799429,24.4353522717955,-1.01073690845387));
#73726=CARTESIAN_POINT('Ctrl Pts',(-22.2945292884817,27.1421276529823,-0.811849997078973));
#73727=CARTESIAN_POINT('Ctrl Pts',(-25.893385689759,26.5482743384945,-0.612963085704084));
#73728=CARTESIAN_POINT('Ctrl Pts',(-27.3391013837051,23.1994931738883,-0.414076174329188));
#73729=CARTESIAN_POINT('Ctrl Pts',(-25.3031862240606,20.1730301196165,-0.215189262954304));
#73730=CARTESIAN_POINT('Ctrl Pts',(-21.6564736253991,20.2499481208034,-0.0163023515794102));
#73731=CARTESIAN_POINT('Ctrl Pts',(-19.7499832756501,23.3595660559294,0.182584559795477));
#73732=CARTESIAN_POINT('Ctrl Pts',(-21.3356181625077,26.6444086947362,0.381471471170368));
#73733=CARTESIAN_POINT('Ctrl Pts',(-24.9563142646179,27.0859841608879,0.580358382545258));
#73734=CARTESIAN_POINT('Ctrl Pts',(-27.2849588485467,24.2785220404165,0.779245293920151));
#73735=CARTESIAN_POINT('Ctrl Pts',(-26.1817249781655,20.801841988501,0.97813220529504));
#73736=CARTESIAN_POINT('Ctrl Pts',(-22.6603910415476,19.850718198994,1.17701911666993));
#73737=CARTESIAN_POINT('Ctrl Pts',(-19.956764366562,22.2991527924536,1.37590602804482));
#73738=CARTESIAN_POINT('Ctrl Pts',(-20.5552486377801,25.89724197051,1.57479293941972));
#73739=CARTESIAN_POINT('Ctrl Pts',(-23.9058875530509,27.3386468461839,1.7736798507946));
#73740=CARTESIAN_POINT('Ctrl Pts',(-26.9297280365722,25.2988385497105,1.9725667621695));
#73741=CARTESIAN_POINT('Ctrl Pts',(-26.8481170633818,21.652227958326,2.17145367354438));
#73742=CARTESIAN_POINT('Ctrl Pts',(-23.7360481983725,19.7497410239209,2.3703405849193));
#73743=CARTESIAN_POINT('Ctrl Pts',(-20.4532488685604,21.3396019349219,2.56922749629416));
#73744=CARTESIAN_POINT('Ctrl Pts',(-20.0163333225597,24.960863312095,2.76811440766907));
#73745=CARTESIAN_POINT('Ctrl Pts',(-22.8267899028154,27.285892982151,2.96700131904394));
#73746=CARTESIAN_POINT('Ctrl Pts',(-26.3020472994952,26.178185808316,3.16588823041884));
#73747=CARTESIAN_POINT('Ctrl Pts',(-27.2486386182868,22.655630765264,3.36477514179371));
#73748=CARTESIAN_POINT('Ctrl Pts',(-24.7967266949296,19.9551572741439,3.56366205316864));
#73749=CARTESIAN_POINT('Ctrl Pts',(-21.1994106991399,20.5582715109011,3.7625489645435));
#73750=CARTESIAN_POINT('Ctrl Pts',(-19.7623190289495,23.9107626276099,3.9614358759184));
#73751=CARTESIAN_POINT('Ctrl Pts',(-21.8060170839828,26.9319755323878,4.16032278729329));
#73752=CARTESIAN_POINT('Ctrl Pts',(-25.4525196286846,26.8456717223558,4.35920969866818));
#73753=CARTESIAN_POINT('Ctrl Pts',(-27.3509999969048,23.7311570815769,4.55809661004306));
#73754=CARTESIAN_POINT('Ctrl Pts',(-25.7569156948398,20.4504064976324,4.75698352141796));
#73755=CARTESIAN_POINT('Ctrl Pts',(-22.1350950400269,20.0181515953885,4.95587043279287));
#73756=CARTESIAN_POINT('Ctrl Pts',(-19.8136841344875,22.8315979808357,5.15475734416772));
#73757=CARTESIAN_POINT('Ctrl Pts',(-20.9258627772252,26.305426966664,5.35364425554262));
#73758=CARTESIAN_POINT('Ctrl Pts',(-24.4496330927626,27.2474842470246,5.55253116691751));
#73759=CARTESIAN_POINT('Ctrl Pts',(-27.1469489275747,24.7920990545517,5.75141807829239));
#73760=CARTESIAN_POINT('Ctrl Pts',(-26.5392057241383,21.1955621987944,5.95030498966732));
#73761=CARTESIAN_POINT('Ctrl Pts',(-23.1848679582852,19.7627861141549,6.1491919010422));
#73762=CARTESIAN_POINT('Ctrl Pts',(-20.1662876358919,21.8103705430376,6.34807881241708));
#73763=CARTESIAN_POINT('Ctrl Pts',(-20.257284139832,25.45675900183,6.54696572379196));
#73764=CARTESIAN_POINT('Ctrl Pts',(-23.3742393982156,27.3512296596596,6.74585263516687));
#73765=CARTESIAN_POINT('Ctrl Pts',(-26.6529358028134,25.7529246066046,6.94473954654172));
#73766=CARTESIAN_POINT('Ctrl Pts',(-27.0805293454125,22.1305506725013,7.14362645791667));
#73767=CARTESIAN_POINT('Ctrl Pts',(-24.2640978143184,19.8127623761288,7.34251336929153));
#73768=CARTESIAN_POINT('Ctrl Pts',(-20.7917029925916,20.9294106458127,7.54140028066643));
#73769=CARTESIAN_POINT('Ctrl Pts',(-19.854181310869,24.4543903978741,7.7402871920413));
#73770=CARTESIAN_POINT('Ctrl Pts',(-22.3130357059231,27.1485441091656,7.93917410341621));
#73771=CARTESIAN_POINT('Ctrl Pts',(-25.9087874651727,26.5361729455757,8.13806101479108));
#73772=CARTESIAN_POINT('Ctrl Pts',(-27.3372455913412,23.1799940859308,8.336947926166));
#73773=CARTESIAN_POINT('Ctrl Pts',(-25.2857781797561,20.1640513452033,8.53583483754088));
#73774=CARTESIAN_POINT('Ctrl Pts',(-21.6395098459112,20.2597403923456,8.73472174891577));
#73775=CARTESIAN_POINT('Ctrl Pts',(-19.7490520360368,23.3791311061275,8.93360866029067));
#73776=CARTESIAN_POINT('Ctrl Pts',(-21.3515751930175,26.6557679013008,9.13249557166553));
#73777=CARTESIAN_POINT('Ctrl Pts',(-24.9744964071453,27.078699376088,9.33138248304043));
#73778=CARTESIAN_POINT('Ctrl Pts',(-27.2886582557006,24.2592873638354,9.5302693944153));
#73779=CARTESIAN_POINT('Ctrl Pts',(-26.1675422084293,20.788332457085,9.72915630579023));
#73780=CARTESIAN_POINT('Ctrl Pts',(-22.6413588578084,19.8553479266951,9.9280432171651));
#73781=CARTESIAN_POINT('Ctrl Pts',(-19.950371732013,22.3176674520504,10.12693012854));
#73782=CARTESIAN_POINT('Ctrl Pts',(-20.567369841566,25.9126281596176,10.3258170399149));
#73783=CARTESIAN_POINT('Ctrl Pts',(-23.9253842366009,27.3367659615458,10.5247039512898));
#73784=CARTESIAN_POINT('Ctrl Pts',(-26.9386844007501,25.2814189648366,10.7235908626646));
#73785=CARTESIAN_POINT('Ctrl Pts',(-26.8383029688828,21.635276794778,10.9224777740396));
#73786=CARTESIAN_POINT('Ctrl Pts',(-23.7164819659429,19.7488349637779,11.1213646854144));
#73787=CARTESIAN_POINT('Ctrl Pts',(-20.4419102068603,21.355573570634,11.3202515967893));
#73788=CARTESIAN_POINT('Ctrl Pts',(-20.0236415003314,24.9790360646143,11.5191385081642));
#73789=CARTESIAN_POINT('Ctrl Pts',(-22.8460293243181,27.2895676327074,11.7180254195391));
#73790=CARTESIAN_POINT('Ctrl Pts',(-26.3155385676017,26.1639856646073,11.916912330914));
#73791=CARTESIAN_POINT('Ctrl Pts',(-27.2439844014783,22.6366045553847,12.1157992422889));
#73792=CARTESIAN_POINT('Ctrl Pts',(-24.7782038238405,19.9487884718166,12.3146861536638));
#73793=CARTESIAN_POINT('Ctrl Pts',(-21.1840401218207,20.5704125054791,12.5135730650387));
#73794=CARTESIAN_POINT('Ctrl Pts',(-19.7642250027464,23.9302568744627,12.7124599764136));
#73795=CARTESIAN_POINT('Ctrl Pts',(-21.8234481805766,26.9409094714972,12.9113468877884));
#73796=CARTESIAN_POINT('Ctrl Pts',(-25.4694581482187,26.8358358211533,13.1102337991634));
#73797=CARTESIAN_POINT('Ctrl Pts',(-27.351880876077,23.7115896993209,13.3091207105382));
#73798=CARTESIAN_POINT('Ctrl Pts',(-25.7409294803771,20.4390883995754,13.5080076219132));
#73799=CARTESIAN_POINT('Ctrl Pts',(-22.116931707613,20.0254831540288,13.706894533288));
#73800=CARTESIAN_POINT('Ctrl Pts',(-19.8100342466141,22.8508421153961,13.9057814446629));
#73801=CARTESIAN_POINT('Ctrl Pts',(-20.9400802713885,26.3188999491173,14.1046683560378));
#73802=CARTESIAN_POINT('Ctrl Pts',(-24.4686532972713,27.2428055488167,14.3035552674127));
#73803=CARTESIAN_POINT('Ctrl Pts',(-27.1532938871325,24.7735680026474,14.5024421787876));
#73804=CARTESIAN_POINT('Ctrl Pts',(-26.5270449588757,21.1802072587197,14.7013290901624));
#73805=CARTESIAN_POINT('Ctrl Pts',(-23.1653761804155,19.7647171739542,14.9002160015374));
#73806=CARTESIAN_POINT('Ctrl Pts',(-20.1573761366472,21.8278131224823,15.0991029129122));
#73807=CARTESIAN_POINT('Ctrl Pts',(-20.2671418314476,25.4736848492971,15.2979898242872));
#73808=CARTESIAN_POINT('Ctrl Pts',(-23.3938078978913,27.3520853564023,15.496876735662));
#73809=CARTESIAN_POINT('Ctrl Pts',(-26.6642333184823,25.7369238398673,15.6957636470369));
#73810=CARTESIAN_POINT('Ctrl Pts',(-27.0731744180464,22.1123967902745,15.8946505584118));
#73811=CARTESIAN_POINT('Ctrl Pts',(-24.2448489985717,19.8091372569833,16.0935374697867));
#73812=CARTESIAN_POINT('Ctrl Pts',(-20.7782483181051,20.943645466884,16.2924243811616));
#73813=CARTESIAN_POINT('Ctrl Pts',(-19.8588844827275,24.4734045655114,16.4913112925365));
#73814=CARTESIAN_POINT('Ctrl Pts',(-22.3315749079519,27.1548652154458,16.6901982039114));
#73815=CARTESIAN_POINT('Ctrl Pts',(-25.9241267425724,26.5239924297687,16.8890851152863));
#73816=CARTESIAN_POINT('Ctrl Pts',(-27.3352894487376,23.160504809326,17.0879720266612));
#73817=CARTESIAN_POINT('Ctrl Pts',(-25.2683241463485,20.1551623005822,17.286858938036));
#73818=CARTESIAN_POINT('Ctrl Pts',(-21.622596698543,20.2696198580485,17.485745849411));
#73819=CARTESIAN_POINT('Ctrl Pts',(-19.7482215231412,23.3987006908139,17.6846327607858));
#73820=CARTESIAN_POINT('Ctrl Pts',(-21.3675904855294,26.6670448158712,17.8835196721607));
#73821=CARTESIAN_POINT('Ctrl Pts',(-24.9926408091195,27.0713210921768,18.0824065835356));
#73822=CARTESIAN_POINT('Ctrl Pts',(-27.2922586001142,24.2400338987816,18.2812934949105));
#73823=CARTESIAN_POINT('Ctrl Pts',(-26.1532900840252,20.7748961128486,18.4801804062854));
#73824=CARTESIAN_POINT('Ctrl Pts',(-22.622350758533,19.860075564415,18.6790673176603));
#73825=CARTESIAN_POINT('Ctrl Pts',(-19.9440744894795,22.3362147734999,18.8779542290352));
#73826=CARTESIAN_POINT('Ctrl Pts',(-20.5795700877444,25.9279517489378,19.0768411404101));
#73827=CARTESIAN_POINT('Ctrl Pts',(-23.9448709796636,27.334784739378,19.275728051785));
#73828=CARTESIAN_POINT('Ctrl Pts',(-26.9475509760259,25.2639535063728,19.4746149631598));
#73829=CARTESIAN_POINT('Ctrl Pts',(-26.8284017454547,21.61837637552,19.6735018745347));
#73830=CARTESIAN_POINT('Ctrl Pts',(-23.6969113286562,19.7480296361044,19.8723887859096));
#73831=CARTESIAN_POINT('Ctrl Pts',(-20.4306539120651,21.3716033623966,20.0712756972845));
#73832=CARTESIAN_POINT('Ctrl Pts',(-20.031043128568,24.9971709562853,20.2701626086594));
#73833=CARTESIAN_POINT('Ctrl Pts',(-22.8652874067917,27.2931431964264,20.4690495200343));
#73834=CARTESIAN_POINT('Ctrl Pts',(-26.3289565593354,26.1497162604744,20.6679364314092));
#73835=CARTESIAN_POINT('Ctrl Pts',(-27.2392323057267,22.6176025559519,20.8668233427841));
#73836=CARTESIAN_POINT('Ctrl Pts',(-24.7596484136882,19.9425151034591,21.065710254159));
#73837=CARTESIAN_POINT('Ctrl Pts',(-21.1687322459583,20.582632461823,21.2645971655339));
#73838=CARTESIAN_POINT('Ctrl Pts',(-19.7662313011976,23.9497410517098,21.4634840769087));
#73839=CARTESIAN_POINT('Ctrl Pts',(-21.8409250351707,26.9497535627429,21.6623709882836));
#73840=CARTESIAN_POINT('Ctrl Pts',(-25.4863458113769,26.8259128563984,21.8612578996585));
#73841=CARTESIAN_POINT('Ctrl Pts',(-27.3526610171945,23.6920180418461,22.0601448110334));
#73842=CARTESIAN_POINT('Ctrl Pts',(-25.7248852159121,20.4278527431975,22.2590317224083));
#73843=CARTESIAN_POINT('Ctrl Pts',(-22.0988063562796,20.032908114332,22.4579186337832));
#73844=CARTESIAN_POINT('Ctrl Pts',(-19.8064834695114,22.8701047833953,22.6568055451581));
#73845=CARTESIAN_POINT('Ctrl Pts',(-20.9543669316176,26.3322995661252,22.8556924565329));
#73846=CARTESIAN_POINT('Ctrl Pts',(-24.487649165391,27.2380290029044,23.0545793679079));
#73847=CARTESIAN_POINT('Ctrl Pts',(-27.1595433709243,24.7550045345219,23.2534662792827));
#73848=CARTESIAN_POINT('Ctrl Pts',(-26.5148053126048,21.1649151216697,23.4523531906577));
#73849=CARTESIAN_POINT('Ctrl Pts',(-23.145894601252,19.766748545362,23.6512401020325));
#73850=CARTESIAN_POINT('Ctrl Pts',(-20.1485545440809,21.8453013442694,23.8501270134075));
#73851=CARTESIAN_POINT('Ctrl Pts',(-20.2770865210912,25.4905597283727,24.0490139247823));
#73852=CARTESIAN_POINT('Ctrl Pts',(-23.4133805431482,27.3528403096971,24.2479008361572));
#73853=CARTESIAN_POINT('Ctrl Pts',(-26.6754483178192,25.7208651292231,24.4467877475321));
#73854=CARTESIAN_POINT('Ctrl Pts',(-27.0657261380023,22.0942810093889,24.645674658907));
#73855=CARTESIAN_POINT('Ctrl Pts',(-24.225581776894,19.8056112722044,24.8445615702819));
#73856=CARTESIAN_POINT('Ctrl Pts',(-20.7648670981191,20.9579493598755,25.0434484816568));
#73857=CARTESIAN_POINT('Ctrl Pts',(-19.8636854706927,24.4923942702399,25.2423353930317));
#73858=CARTESIAN_POINT('Ctrl Pts',(-22.3501464036785,27.1610908054883,25.4412223044065));
#73859=CARTESIAN_POINT('Ctrl Pts',(-25.9394031147813,26.5117331116385,25.6401092157814));
#73860=CARTESIAN_POINT('Ctrl Pts',(-27.3332330090641,23.1410258646715,25.8389961271563));
#73861=CARTESIAN_POINT('Ctrl Pts',(-25.250824583827,20.146363213449,26.0378830385312));
#73862=CARTESIAN_POINT('Ctrl Pts',(-21.6057346362272,20.2795862709453,26.2367699499061));
#73863=CARTESIAN_POINT('Ctrl Pts',(-19.7474917499884,23.4182742634268,26.435656861281));
#73864=CARTESIAN_POINT('Ctrl Pts',(-21.3836636326193,26.6782391924832,26.6345437726559));
#73865=CARTESIAN_POINT('Ctrl Pts',(-25.0107469577146,27.0638494048605,26.8334306840308));
#73866=CARTESIAN_POINT('Ctrl Pts',(-27.2957598468497,24.2207623439047,27.0323175954057));
#73867=CARTESIAN_POINT('Ctrl Pts',(-26.1389688684423,20.7615329559886,27.2312045067806));
#73868=CARTESIAN_POINT('Ctrl Pts',(-22.6033674629925,19.864901658791,27.4300914181554));
#73869=CARTESIAN_POINT('Ctrl Pts',(-19.9378723987674,22.3547929966136,27.6289783295304));
#73870=CARTESIAN_POINT('Ctrl Pts',(-20.5918498216416,25.9432147279969,27.8278652409052));
#73871=CARTESIAN_POINT('Ctrl Pts',(-23.9643458145628,27.3326987088365,28.0267521522802));
#73872=CARTESIAN_POINT('Ctrl Pts',(-26.9563302678041,25.2464511781227,28.225639063655));
#73873=CARTESIAN_POINT('Ctrl Pts',(-26.8184084811151,21.601511021257,28.4245259750299));
#73874=CARTESIAN_POINT('Ctrl Pts',(-23.6773465753398,19.7473555135675,28.6234128864048));
#73875=CARTESIAN_POINT('Ctrl Pts',(-20.4194618342357,21.387633386982,28.8222997977797));
#73876=CARTESIAN_POINT('Ctrl Pts',(-20.0385728453635,25.0153760766652,29.0211867091546));
#73877=CARTESIAN_POINT('Ctrl Pts',(-22.8844978638131,27.296414565311,29.2200736205295));
#73878=CARTESIAN_POINT('Ctrl Pts',(-26.3424251341972,26.135765169103,29.4189605319043));
#73879=CARTESIAN_POINT('Ctrl Pts',(-27.2341477796763,22.5978934450653,29.6178474432793));
#73880=CARTESIAN_POINT('Ctrl Pts',(-24.7415051702057,19.9377250765665,29.8167343546542));
#73881=CARTESIAN_POINT('Ctrl Pts',(-21.1526397381544,20.5922624614815,30.0156212660291));
#73882=CARTESIAN_POINT('Ctrl Pts',(-19.7700134152175,23.9746450020287,30.2145081774039));
#73883=CARTESIAN_POINT('Ctrl Pts',(-21.1596874956222,25.9551180584479,30.3470994516539));
#73884=CARTESIAN_POINT('Ctrl Pts',(-22.1199161766065,26.4317607972602,30.4133950887789));
#73885=CARTESIAN_POINT('',(-21.6764439629923,20.9249433714536,30.0016351447898));
#73886=CARTESIAN_POINT('Ctrl Pts',(-21.6746633416192,20.9227079640045,30.));
#73887=CARTESIAN_POINT('Ctrl Pts',(-21.6162991313229,20.9552163909426,30.0000000000001));
#73888=CARTESIAN_POINT('Ctrl Pts',(-21.5591356012991,20.9896046533105,30.0000000000001));
#73889=CARTESIAN_POINT('Ctrl Pts',(-21.503273460136,21.0258485698887,30.0000000000001));
#73890=CARTESIAN_POINT('Ctrl Pts',(-21.4177259766631,21.0813526338203,30.));
#73891=CARTESIAN_POINT('Ctrl Pts',(-21.3352292623413,21.1412057073851,30.));
#73892=CARTESIAN_POINT('Ctrl Pts',(-21.2558644350544,21.2050026175341,30.));
#73893=CARTESIAN_POINT('Ctrl Pts',(-21.1739425301015,21.2708550182534,30.));
#73894=CARTESIAN_POINT('Ctrl Pts',(-21.0953570390573,21.3409098039315,30.));
#73895=CARTESIAN_POINT('Ctrl Pts',(-21.020216898794,21.4147745496451,30.));
#73896=CARTESIAN_POINT('Ctrl Pts',(-20.9451050091674,21.4886115242355,30.));
#73897=CARTESIAN_POINT('Ctrl Pts',(-20.8734354129643,21.5662562353673,30.));
#73898=CARTESIAN_POINT('Ctrl Pts',(-20.80534380024,21.6473612898953,30.));
#73899=CARTESIAN_POINT('Ctrl Pts',(-20.7823042330275,21.6748041023109,30.));
#73900=CARTESIAN_POINT('Ctrl Pts',(-20.7596745620235,21.7026434173923,30.));
#73901=CARTESIAN_POINT('Ctrl Pts',(-20.7374608883305,21.7308667324253,30.));
#73902=CARTESIAN_POINT('Ctrl Pts',(-20.7255551836852,21.7459933817826,30.));
#73903=CARTESIAN_POINT('Ctrl Pts',(-20.7137674457841,21.7612325178852,30.));
#73904=CARTESIAN_POINT('Ctrl Pts',(-20.7021130296544,21.7765629307075,30.));
#73905=CARTESIAN_POINT('Ctrl Pts',(-20.6363129063594,21.8631175073289,30.));
#73906=CARTESIAN_POINT('Ctrl Pts',(-20.5746612361573,21.9527016157851,30.));
#73907=CARTESIAN_POINT('Ctrl Pts',(-20.5172553062057,22.044887933698,30.));
#73908=CARTESIAN_POINT('Ctrl Pts',(-20.4582421259944,22.1396552825868,30.));
#73909=CARTESIAN_POINT('Ctrl Pts',(-20.4037151310162,22.2371731196096,29.9999999999999));
#73910=CARTESIAN_POINT('Ctrl Pts',(-20.3538094801165,22.3370248209967,30.));
#73911=CARTESIAN_POINT('Ctrl Pts',(-20.3039038292169,22.4368765223838,30.));
#73912=CARTESIAN_POINT('Ctrl Pts',(-20.2586189951566,22.539062873371,30.));
#73913=CARTESIAN_POINT('Ctrl Pts',(-20.2181277537056,22.6432039299912,29.9999999999999));
#73914=CARTESIAN_POINT('Ctrl Pts',(-20.1978995014436,22.6952297876499,29.9999999999999));
#73915=CARTESIAN_POINT('Ctrl Pts',(-20.1788682282719,22.7477439827443,30.));
#73916=CARTESIAN_POINT('Ctrl Pts',(-20.1610596298732,22.8007016284567,30.));
#73917=CARTESIAN_POINT('Ctrl Pts',(-20.1479433637699,22.8397056285367,30.));
#73918=CARTESIAN_POINT('Ctrl Pts',(-20.1354903970461,22.8789502128354,30.));
#73919=CARTESIAN_POINT('Ctrl Pts',(-20.1237120651554,22.9184178619925,30.));
#73920=CARTESIAN_POINT('Ctrl Pts',(-20.118220135111,22.9368206010388,29.9999999999999));
#73921=CARTESIAN_POINT('Ctrl Pts',(-20.1128766266359,22.9552662915841,29.9999999999999));
#73922=CARTESIAN_POINT('Ctrl Pts',(-20.1076860627291,22.9737395492117,29.9999999999999));
#73923=CARTESIAN_POINT('Ctrl Pts',(-20.0765757289063,23.084461471129,29.9999999999999));
#73924=CARTESIAN_POINT('Ctrl Pts',(-20.0509141219901,23.1963121778044,29.9999999999999));
#73925=CARTESIAN_POINT('Ctrl Pts',(-20.0308372856757,23.3088624101692,30.));
#73926=CARTESIAN_POINT('Ctrl Pts',(-20.0108369308768,23.4209838891087,30.));
#73927=CARTESIAN_POINT('Ctrl Pts',(-19.9963783905913,23.5338004229941,29.9999999999999));
#73928=CARTESIAN_POINT('Ctrl Pts',(-19.9876380605889,23.6469168071079,29.9999999999999));
#73929=CARTESIAN_POINT('Ctrl Pts',(-19.9799173108421,23.7468378963304,30.));
#73930=CARTESIAN_POINT('Ctrl Pts',(-19.9766588595465,23.8469937496122,29.9999999999999));
#73931=CARTESIAN_POINT('Ctrl Pts',(-19.9780163121772,23.9471230379573,29.9999999999999));
#73932=CARTESIAN_POINT('Ctrl Pts',(-19.9790735041223,24.0251043057529,29.9999999999999));
#73933=CARTESIAN_POINT('Ctrl Pts',(-19.9829310173974,24.1030697257942,29.9999999999999));
#73934=CARTESIAN_POINT('Ctrl Pts',(-19.9895131648371,24.1809217806588,29.9999999999999));
#73935=CARTESIAN_POINT('Ctrl Pts',(-19.9915591683848,24.2051214179212,29.9999999999999));
#73936=CARTESIAN_POINT('Ctrl Pts',(-19.9938685241954,24.2293101033187,30.));
#73937=CARTESIAN_POINT('Ctrl Pts',(-19.9964392042166,24.2534849041834,30.));
#73938=CARTESIAN_POINT('Ctrl Pts',(-19.9988085349521,24.2757662065003,30.));
#73939=CARTESIAN_POINT('Ctrl Pts',(-20.0014006070192,24.2980408294194,30.));
#73940=CARTESIAN_POINT('Ctrl Pts',(-20.0042097151299,24.3202756502583,30.));
#73941=CARTESIAN_POINT('Ctrl Pts',(-20.0183122567051,24.4319009323555,30.));
#73942=CARTESIAN_POINT('Ctrl Pts',(-20.0378917318368,24.5426515255195,30.));
#73943=CARTESIAN_POINT('Ctrl Pts',(-20.0626333972095,24.6522326886167,29.9999999999999));
#73944=CARTESIAN_POINT('Ctrl Pts',(-20.0878348626783,24.7638503124199,29.9999999999999));
#73945=CARTESIAN_POINT('Ctrl Pts',(-20.1183922903517,24.8742552772806,30.));
#73946=CARTESIAN_POINT('Ctrl Pts',(-20.1540278013711,24.9831449157989,30.));
#73947=CARTESIAN_POINT('Ctrl Pts',(-20.1903931760521,25.0942647619953,30.));
#73948=CARTESIAN_POINT('Ctrl Pts',(-20.2320469100759,25.2038073279202,29.9999999999999));
#73949=CARTESIAN_POINT('Ctrl Pts',(-20.2787482606345,25.3114493816107,29.9999999999999));
#73950=CARTESIAN_POINT('Ctrl Pts',(-20.3172931777526,25.4002916525151,30.));
#73951=CARTESIAN_POINT('Ctrl Pts',(-20.3592776204364,25.487839474204,30.));
#73952=CARTESIAN_POINT('Ctrl Pts',(-20.4045921510452,25.5739046343225,30.));
#73953=CARTESIAN_POINT('Ctrl Pts',(-20.4146318244921,25.5929728248376,30.));
#73954=CARTESIAN_POINT('Ctrl Pts',(-20.4248350475835,25.6119682021458,30.));
#73955=CARTESIAN_POINT('Ctrl Pts',(-20.4352007754019,25.6308886550293,30.));
#73956=CARTESIAN_POINT('Ctrl Pts',(-20.4443567625954,25.6476009811999,30.));
#73957=CARTESIAN_POINT('Ctrl Pts',(-20.4536352337179,25.6642469447489,30.));
#73958=CARTESIAN_POINT('Ctrl Pts',(-20.4630327056216,25.6808210834781,30.));
#73959=CARTESIAN_POINT('Ctrl Pts',(-20.5226722799696,25.7860062427551,30.));
#73960=CARTESIAN_POINT('Ctrl Pts',(-20.5871297547875,25.8883528199085,30.));
#73961=CARTESIAN_POINT('Ctrl Pts',(-20.6561268215069,25.9875227195612,30.));
#73962=CARTESIAN_POINT('Ctrl Pts',(-20.7250424718538,26.0865755989711,30.));
#73963=CARTESIAN_POINT('Ctrl Pts',(-20.7984873863524,26.1824601011885,30.));
#73964=CARTESIAN_POINT('Ctrl Pts',(-20.8762341567312,26.2748250760474,30.));
#73965=CARTESIAN_POINT('Ctrl Pts',(-20.9113897218986,26.3165907066584,30.));
#73966=CARTESIAN_POINT('Ctrl Pts',(-20.9474255175054,26.3576364424982,30.));
#73967=CARTESIAN_POINT('Ctrl Pts',(-20.9843235564789,26.3979281736167,30.));
#73968=CARTESIAN_POINT('Ctrl Pts',(-21.0055405379232,26.4210965840603,30.));
#73969=CARTESIAN_POINT('Ctrl Pts',(-21.0270476541474,26.4440206793492,30.));
#73970=CARTESIAN_POINT('Ctrl Pts',(-21.0488151960231,26.4666667341842,30.));
#73971=CARTESIAN_POINT('Ctrl Pts',(-21.1342995706145,26.5556011598344,30.));
#73972=CARTESIAN_POINT('Ctrl Pts',(-21.2238508060944,26.6403121960061,30.));
#73973=CARTESIAN_POINT('Ctrl Pts',(-21.3172138848137,26.7204449989692,30.));
#73974=CARTESIAN_POINT('Ctrl Pts',(-21.4093682581618,26.7995403795307,30.));
#73975=CARTESIAN_POINT('Ctrl Pts',(-21.5052368954238,26.8741760552448,30.));
#73976=CARTESIAN_POINT('Ctrl Pts',(-21.6046172148253,26.943984558935,30.));
#73977=CARTESIAN_POINT('Ctrl Pts',(-21.6688134411653,26.9890784218883,30.0000000000001));
#73978=CARTESIAN_POINT('Ctrl Pts',(-21.7344758343746,27.0321574881717,30.));
#73979=CARTESIAN_POINT('Ctrl Pts',(-21.801558056363,27.073114526145,30.));
#73980=CARTESIAN_POINT('Ctrl Pts',(-21.7179950055095,20.8990358449182,30.));
#73981=CARTESIAN_POINT('Ctrl Pts',(-21.7045931386319,20.9082978835791,30.0005450482633));
#73982=CARTESIAN_POINT('Ctrl Pts',(-21.6912615023449,20.917661543581,30.0010900965265));
#73983=CARTESIAN_POINT('Ctrl Pts',(-21.6780016295741,20.9271257482523,30.0016351447898));
#73984=CARTESIAN_POINT('Ctrl Pts',(-21.7974962932627,27.0786396387202,-75.));
#73985=CARTESIAN_POINT('Ctrl Pts',(-21.7283390717874,27.0367793117585,-75.));
#73986=CARTESIAN_POINT('Ctrl Pts',(-21.6606954899468,26.9927043362926,-75.));
#73987=CARTESIAN_POINT('Ctrl Pts',(-21.5946811745421,26.9464145021147,-75.));
#73988=CARTESIAN_POINT('Ctrl Pts',(-21.4964605389816,26.8775413053685,-75.));
#73989=CARTESIAN_POINT('Ctrl Pts',(-21.4018447932092,26.8037666197796,-75.));
#73990=CARTESIAN_POINT('Ctrl Pts',(-21.310988531103,26.7255041388125,-75.));
#73991=CARTESIAN_POINT('Ctrl Pts',(-21.2173740700917,26.6448657787996,-75.));
#73992=CARTESIAN_POINT('Ctrl Pts',(-21.1277502293408,26.5594622355224,-75.));
#73993=CARTESIAN_POINT('Ctrl Pts',(-21.0423302684772,26.4697105300495,-75.));
#73994=CARTESIAN_POINT('Ctrl Pts',(-20.9569103076136,26.3799588245765,-75.));
#73995=CARTESIAN_POINT('Ctrl Pts',(-20.8756938384798,26.2858579924122,-75.));
#73996=CARTESIAN_POINT('Ctrl Pts',(-20.7989446998575,26.1878035336579,-75.));
#73997=CARTESIAN_POINT('Ctrl Pts',(-20.7738469905589,26.1557387789854,-75.));
#73998=CARTESIAN_POINT('Ctrl Pts',(-20.7492274240551,26.123251132326,-75.));
#73999=CARTESIAN_POINT('Ctrl Pts',(-20.7250965081235,26.0903541909719,-75.));
#74000=CARTESIAN_POINT('Ctrl Pts',(-20.7122572410852,26.0728508099985,-75.));
#74001=CARTESIAN_POINT('Ctrl Pts',(-20.6995540939926,26.0552282695939,-75.));
#74002=CARTESIAN_POINT('Ctrl Pts',(-20.6870042731299,26.0375110019382,-75.));
#74003=CARTESIAN_POINT('Ctrl Pts',(-20.6176725248015,25.9396315855219,-75.));
#74004=CARTESIAN_POINT('Ctrl Pts',(-20.5529233324656,25.8387394985084,-75.));
#74005=CARTESIAN_POINT('Ctrl Pts',(-20.4929223796897,25.735229157897,-75.));
#74006=CARTESIAN_POINT('Ctrl Pts',(-20.4330471356119,25.6319356830113,-75.));
#74007=CARTESIAN_POINT('Ctrl Pts',(-20.3778999559587,25.5260340211465,-75.));
#74008=CARTESIAN_POINT('Ctrl Pts',(-20.3276933492384,25.4178965871798,-75.));
#74009=CARTESIAN_POINT('Ctrl Pts',(-20.2785647484585,25.3120810148924,-75.));
#74010=CARTESIAN_POINT('Ctrl Pts',(-20.2341667224708,25.2041238330088,-75.));
#74011=CARTESIAN_POINT('Ctrl Pts',(-20.1947470562131,25.0943679175727,-75.));
#74012=CARTESIAN_POINT('Ctrl Pts',(-20.1639433742703,25.0086014301469,-75.));
#74013=CARTESIAN_POINT('Ctrl Pts',(-20.1361805474816,24.9217363466615,-75.));
#74014=CARTESIAN_POINT('Ctrl Pts',(-20.1115989699483,24.8339383046586,-75.));
#74015=CARTESIAN_POINT('Ctrl Pts',(-20.1046926632002,24.8092710427982,-75.));
#74016=CARTESIAN_POINT('Ctrl Pts',(-20.0980375924697,24.7845301610143,-75.));
#74017=CARTESIAN_POINT('Ctrl Pts',(-20.0916371627657,24.7597193987049,-75.));
#74018=CARTESIAN_POINT('Ctrl Pts',(-20.0876060935858,24.7440932761005,-75.));
#74019=CARTESIAN_POINT('Ctrl Pts',(-20.0836783296642,24.7284483005329,-75.));
#74020=CARTESIAN_POINT('Ctrl Pts',(-20.0798548286623,24.7127873583955,-75.));
#74021=CARTESIAN_POINT('Ctrl Pts',(-20.0526442063565,24.6013334889587,-75.));
#74022=CARTESIAN_POINT('Ctrl Pts',(-20.0307017298995,24.4890392161558,-75.));
#74023=CARTESIAN_POINT('Ctrl Pts',(-20.0142207624146,24.376241682378,-75.));
#74024=CARTESIAN_POINT('Ctrl Pts',(-19.9981827954567,24.2664760923835,-75.));
#74025=CARTESIAN_POINT('Ctrl Pts',(-19.9873166714761,24.1562332280512,-75.));
#74026=CARTESIAN_POINT('Ctrl Pts',(-19.9818488412096,24.0458250777531,-75.));
#74027=CARTESIAN_POINT('Ctrl Pts',(-19.9765152055089,23.9381266263781,-75.));
#74028=CARTESIAN_POINT('Ctrl Pts',(-19.9763181341626,23.8302703368621,-75.));
#74029=CARTESIAN_POINT('Ctrl Pts',(-19.981514471678,23.7225562298032,-75.));
#74030=CARTESIAN_POINT('Ctrl Pts',(-19.9849161460783,23.6520434273831,-75.));
#74031=CARTESIAN_POINT('Ctrl Pts',(-19.9906302912664,23.5815917845486,-75.));
#74032=CARTESIAN_POINT('Ctrl Pts',(-19.9986155805899,23.5112909714078,-75.));
#74033=CARTESIAN_POINT('Ctrl Pts',(-20.003199291308,23.4709369431902,-75.));
#74034=CARTESIAN_POINT('Ctrl Pts',(-20.0085314577195,23.4306326838506,-75.));
#74035=CARTESIAN_POINT('Ctrl Pts',(-20.0146051507011,23.3903958166286,-75.));
#74036=CARTESIAN_POINT('Ctrl Pts',(-20.0167180048619,23.3763986270134,-75.));
#74037=CARTESIAN_POINT('Ctrl Pts',(-20.0189204354708,23.3624109556746,-75.));
#74038=CARTESIAN_POINT('Ctrl Pts',(-20.0212104245034,23.3484431127975,-75.));
#74039=CARTESIAN_POINT('Ctrl Pts',(-20.0392175037149,23.2386085024456,-75.));
#74040=CARTESIAN_POINT('Ctrl Pts',(-20.0626585270014,23.1298348279055,-75.));
#74041=CARTESIAN_POINT('Ctrl Pts',(-20.0912811900811,23.0224446539065,-75.));
#74042=CARTESIAN_POINT('Ctrl Pts',(-20.1201672662221,22.9140661730397,-75.));
#74043=CARTESIAN_POINT('Ctrl Pts',(-20.1543313129296,22.8070959786198,-75.));
#74044=CARTESIAN_POINT('Ctrl Pts',(-20.1935634412397,22.7018862508728,-75.));
#74045=CARTESIAN_POINT('Ctrl Pts',(-20.2325205383007,22.5974140809409,-75.));
#74046=CARTESIAN_POINT('Ctrl Pts',(-20.2764755197019,22.4946770802421,-75.));
#74047=CARTESIAN_POINT('Ctrl Pts',(-20.3252627503745,22.3940514342329,-75.));
#74048=CARTESIAN_POINT('Ctrl Pts',(-20.3617588392728,22.3187767676538,-75.));
#74049=CARTESIAN_POINT('Ctrl Pts',(-20.4009599336471,22.2446842016851,-75.));
#74050=CARTESIAN_POINT('Ctrl Pts',(-20.4428084227994,22.1719463370744,-75.));
#74051=CARTESIAN_POINT('Ctrl Pts',(-20.4518866169818,22.1561673096178,-75.));
#74052=CARTESIAN_POINT('Ctrl Pts',(-20.4610894266242,22.1404520873299,-75.));
#74053=CARTESIAN_POINT('Ctrl Pts',(-20.4704163156628,22.1248025261853,-75.));
#74054=CARTESIAN_POINT('Ctrl Pts',(-20.4793717463345,22.1097762340002,-75.));
#74055=CARTESIAN_POINT('Ctrl Pts',(-20.488436133018,22.0948196004795,-75.));
#74056=CARTESIAN_POINT('Ctrl Pts',(-20.4976085941122,22.0799340839653,-75.));
#74057=CARTESIAN_POINT('Ctrl Pts',(-20.5553350202004,21.986252828736,-75.));
#74058=CARTESIAN_POINT('Ctrl Pts',(-20.6173400240107,21.895383719604,-75.));
#74059=CARTESIAN_POINT('Ctrl Pts',(-20.6834436914446,21.8076804756593,-75.));
#74060=CARTESIAN_POINT('Ctrl Pts',(-20.7483240396607,21.7216002742469,-75.));
#74061=CARTESIAN_POINT('Ctrl Pts',(-20.8171533747666,21.6385693274253,-75.));
#74062=CARTESIAN_POINT('Ctrl Pts',(-20.8897908208752,21.5589625397611,-75.));
#74063=CARTESIAN_POINT('Ctrl Pts',(-20.9134500760797,21.5330332511329,-75.));
#74064=CARTESIAN_POINT('Ctrl Pts',(-20.9375135358778,21.5074675941264,-75.));
#74065=CARTESIAN_POINT('Ctrl Pts',(-20.961976855156,21.4822796143524,-75.));
#74066=CARTESIAN_POINT('Ctrl Pts',(-20.9752011214181,21.4686636145224,-75.));
#74067=CARTESIAN_POINT('Ctrl Pts',(-20.9885422392495,21.4551579899628,-75.));
#74068=CARTESIAN_POINT('Ctrl Pts',(-21.0019995485501,21.4417650307609,-75.));
#74069=CARTESIAN_POINT('Ctrl Pts',(-21.0162043601948,21.4276281436182,-75.));
#74070=CARTESIAN_POINT('Ctrl Pts',(-21.0305328467645,21.4136225861381,-75.));
#74071=CARTESIAN_POINT('Ctrl Pts',(-21.0449800556171,21.3997543930508,-75.));
#74072=CARTESIAN_POINT('Ctrl Pts',(-21.1211701753906,21.3266178236865,-74.9999999999999));
#74073=CARTESIAN_POINT('Ctrl Pts',(-21.2006943104828,21.257263966122,-75.));
#74074=CARTESIAN_POINT('Ctrl Pts',(-21.2834081447689,21.1920390844365,-75.));
#74075=CARTESIAN_POINT('Ctrl Pts',(-21.3638718580856,21.128588559789,-75.));
#74076=CARTESIAN_POINT('Ctrl Pts',(-21.4473546333109,21.0690451037359,-75.));
#74077=CARTESIAN_POINT('Ctrl Pts',(-21.533742621169,21.0137725358826,-75.));
#74078=CARTESIAN_POINT('Ctrl Pts',(-21.5811798388471,20.9834213620921,-75.));
#74079=CARTESIAN_POINT('Ctrl Pts',(-21.6294933571473,20.9543588180351,-75.));
#74080=CARTESIAN_POINT('Ctrl Pts',(-21.6786659999551,20.9266516823435,-75.));
#74081=CARTESIAN_POINT('Origin',(-23.5502525316942,23.5502525316942,30.));
#74082=CARTESIAN_POINT('Origin',(-23.5502525316942,23.5502525316942,-75.));
#74096=UNCERTAINTY_MEASURE_WITH_UNIT(LENGTH_MEASURE(0.01),#74104,
'DISTANCE_ACCURACY_VALUE',
'Maximum model space distance between geometric entities at asserted c
onnectivities');
#74097=UNCERTAINTY_MEASURE_WITH_UNIT(LENGTH_MEASURE(0.01),#74104,
'DISTANCE_ACCURACY_VALUE',
'Maximum model space distance between geometric entities at asserted c
onnectivities');
#74102=(
GEOMETRIC_REPRESENTATION_CONTEXT(3)
GLOBAL_UNCERTAINTY_ASSIGNED_CONTEXT((#74096))
GLOBAL_UNIT_ASSIGNED_CONTEXT((#74104,#74106,#74107))
REPRESENTATION_CONTEXT('','3D')
);
#74103=(
GEOMETRIC_REPRESENTATION_CONTEXT(3)
GLOBAL_UNCERTAINTY_ASSIGNED_CONTEXT((#74097))
GLOBAL_UNIT_ASSIGNED_CONTEXT((#74104,#74106,#74107))
REPRESENTATION_CONTEXT('','3D')
);
#74104=(
LENGTH_UNIT()
NAMED_UNIT(*)
SI_UNIT(.MILLI.,.METRE.)
);
#74106=(
NAMED_UNIT(*)
PLANE_ANGLE_UNIT()
SI_UNIT($,.RADIAN.)
);
#74107=(
NAMED_UNIT(*)
SI_UNIT($,.STERADIAN.)
SOLID_ANGLE_UNIT()
);
#74112=SHAPE_DEFINITION_REPRESENTATION(#74117,#74131);
#74117=PRODUCT_DEFINITION_SHAPE('',$,#74137);
#74131=SHAPE_REPRESENTATION('',(#4845),#74102);
#74132=PRODUCT_DEFINITION_CONTEXT('part definition',#74149,'design');
#74137=PRODUCT_DEFINITION('Rod_01','Rod_01',#74142,#74132);
#74142=PRODUCT_DEFINITION_FORMATION('',$,#74155);
#74149=APPLICATION_CONTEXT(
'Core Data for Automotive Mechanical Design Process');
#74150=PRODUCT_CONTEXT('part definition',#74149,'mechanical');
#74155=PRODUCT('Rod_01','Rod_01',$,(#74150));
#74159=PRESENTATION_STYLE_ASSIGNMENT((#74163));
#74163=SURFACE_STYLE_USAGE(.BOTH.,#74167);
#74167=SURFACE_SIDE_STYLE('',(#74171));
#74171=SURFACE_STYLE_FILL_AREA(#74175);
#74175=FILL_AREA_STYLE('Opaque(160,160,160)',(#74179));
#74179=FILL_AREA_STYLE_COLOUR('Opaque(160,160,160)',#74183);
#74183=COLOUR_RGB('Opaque(160,160,160)', 0.40784314, 0.44705882, 0.49803922);
ENDSEC;
END-ISO-10303-21;
